ISO-10303-21;
HEADER;
FILE_DESCRIPTION (('STEP AP203'),
    '1' );
FILE_NAME ('Measuring Tape_Varsayılan.step',
    '2026-10-08T23:54:15',
    ( '' ),
    ( '' ),
    'SwSTEP 2.0',
    'SolidWorks 2024',
    '' );
FILE_SCHEMA (( 'AUTOMOTIVE_DESIGN' ));
ENDSEC;

DATA;
#4=CARTESIAN_POINT ( 'NONE',  ( -80.94237186737068157, -25.14918324602283661, 7.008237357988867267 ) ) ;
#5=EDGE_CURVE ( 'NONE', #2549, #11314, #80925, .T. ) ;
#6=AXIS2_PLACEMENT_3D ( 'NONE', #5128, #50815, #66059 ) ;
#7=CARTESIAN_POINT ( 'NONE',  ( -51.65200394065919909, -23.73791477778912196, 11.05961554403170766 ) ) ;
#8=CARTESIAN_POINT ( 'NONE',  ( 6.361473516681357410, -20.28576754457002451, 11.49999999999999645 ) ) ;
#11=EDGE_LOOP ( 'NONE', ( #61947, #2008, #96501, #28835 ) ) ;
#12=CARTESIAN_POINT ( 'NONE',  ( -5.848988146064017180, 21.40304369876291446, 11.49999999999998934 ) ) ;
#13=CARTESIAN_POINT ( 'NONE',  ( -4.704028875484805639, -20.06825252194306941, 11.49999999999998934 ) ) ;
#15=ORIENTED_EDGE ( 'NONE', *, *, #21720, .F. ) ;
#16=ORIENTED_EDGE ( 'NONE', *, *, #57693, .T. ) ;
#17=DIRECTION ( 'NONE',  ( 1.000000000000000000, 3.773278334444166432E-23, 8.201307841325785021E-29 ) ) ;
#18=CARTESIAN_POINT ( 'NONE',  ( -39.73355216781377663, -25.15155473006780795, 3.010709736661470348 ) ) ;
#20=CARTESIAN_POINT ( 'NONE',  ( -91.51201375565671015, -24.15543982623907482, -0.2315651400026614848 ) ) ;
#21=VERTEX_POINT ( 'NONE', #59747 ) ;
#22=CARTESIAN_POINT ( 'NONE',  ( -121.6228709571500559, -23.47596703998600631, 11.44779298504227683 ) ) ;
#23=CARTESIAN_POINT ( 'NONE',  ( -44.52287095715004739, -23.94994826722564696, -0.6494450866342734718 ) ) ;
#24=CARTESIAN_POINT ( 'NONE',  ( 9.770152518076534065, 18.40777400073588410, -1.500000000000002220 ) ) ;
#25=CARTESIAN_POINT ( 'NONE',  ( 21.67628855941699939, -2.339797445609365756, 11.49999999999999645 ) ) ;
#28=CARTESIAN_POINT ( 'NONE',  ( 1.786768808452938950, -22.39398889530128756, -1.500000000000002220 ) ) ;
#29=CARTESIAN_POINT ( 'NONE',  ( -118.5885948168727850, -24.51419770103160189, 9.386484678747168076 ) ) ;
#30=ORIENTED_EDGE ( 'NONE', *, *, #89645, .T. ) ;
#32=CARTESIAN_POINT ( 'NONE',  ( -51.15979583992254476, -25.14713903054791189, 3.043340899898625551 ) ) ;
#35=ORIENTED_EDGE ( 'NONE', *, *, #13828, .T. ) ;
#36=B_SPLINE_CURVE_WITH_KNOTS ( 'NONE', 3,
 ( #15893, #77778, #86413, #8288 ),
 .UNSPECIFIED., .F., .F.,
 ( 4, 4 ),
 ( 0.000000000000000000, 1.000000000000000000 ),
 .UNSPECIFIED. ) ;
#37=EDGE_CURVE ( 'NONE', #33217, #73517, #53079, .T. ) ;
#38=CARTESIAN_POINT ( 'NONE',  ( -21.27170209485220198, -2.091907790468015005, -1.500000000000002220 ) ) ;
#40=CARTESIAN_POINT ( 'NONE',  ( -19.40065202112720755, 8.109199488025859992, -1.500000000000002220 ) ) ;
#42=CARTESIAN_POINT ( 'NONE',  ( -110.8023840715768671, -25.20836527976632624, 3.390575860289634313 ) ) ;
#43=CARTESIAN_POINT ( 'NONE',  ( -49.64804092875103692, -25.07480650350090556, 7.411405559915849928 ) ) ;
#44=CARTESIAN_POINT ( 'NONE',  ( 21.11370014442628218, -6.196533921283487345, -1.500000000000002220 ) ) ;
#45=CARTESIAN_POINT ( 'NONE',  ( -52.62287095715006302, -23.94994826722515668, -0.6494450866351718643 ) ) ;
#46=ORIENTED_EDGE ( 'NONE', *, *, #67580, .T. ) ;
#48=B_SPLINE_CURVE_WITH_KNOTS ( 'NONE', 3,
 ( #59465, #45731, #6661, #91892, #14263, #52846 ),
 .UNSPECIFIED., .F., .F.,
 ( 4, 2, 4 ),
 ( 6.384118695835943749E-06, 0.001386860460836991790, 0.002767336802978147530 ),
 .UNSPECIFIED. ) ;
#50=FACE_OUTER_BOUND ( 'NONE', #1014, .T. ) ;
#51=CARTESIAN_POINT ( 'NONE',  ( 2.550444227103870531, -20.70361394434535285, 11.49999999999999645 ) ) ;
#53=ADVANCED_FACE ( 'NONE', ( #51630 ), #45520, .T. ) ;
#57=CARTESIAN_POINT ( 'NONE',  ( -0.07181233839971890021, -22.12033284636826025, 9.440663514584143101 ) ) ;
#58=CARTESIAN_POINT ( 'NONE',  ( 6.557060941508195739, 20.25493142521265355, 11.49999999999998934 ) ) ;
#59=CARTESIAN_POINT ( 'NONE',  ( -31.24388727629349916, -25.30630219089158928, 5.533642405256624208 ) ) ;
#60=CARTESIAN_POINT ( 'NONE',  ( -107.6235340483385130, -24.66019654487200441, 8.947790411086112172 ) ) ;
#61=AXIS2_PLACEMENT_3D ( 'NONE', #34218, #56566, #41326 ) ;
#62=CARTESIAN_POINT ( 'NONE',  ( -29.55620429048338949, -23.39166825546095296, 11.44779303307417706 ) ) ;
#64=CARTESIAN_POINT ( 'NONE',  ( -19.74168752133572724, 10.86179948771369297, -1.500000000000002220 ) ) ;
#65=CARTESIAN_POINT ( 'NONE',  ( -121.6228709571500417, -29.50250786944525672, 11.44777988621622811 ) ) ;
#68=CARTESIAN_POINT ( 'NONE',  ( 12.01011565470214393, -15.49198969801113890, 11.49999999999999645 ) ) ;
#69=DIRECTION ( 'NONE',  ( -3.773278334453079030E-23, 0.9999999999976377785, 2.173523156925979128E-06 ) ) ;
#71=ADVANCED_FACE ( 'NONE', ( #37402 ), #6941, .F. ) ;
#72=ORIENTED_EDGE ( 'NONE', *, *, #32563, .F. ) ;
#73=CARTESIAN_POINT ( 'NONE',  ( -88.59478516332772813, -23.96169478059713853, 10.65365249895717703 ) ) ;
#74=CARTESIAN_POINT ( 'NONE',  ( -124.7734663299911091, -25.37177631213229390, 5.922859790593148155 ) ) ;
#75=FACE_OUTER_BOUND ( 'NONE', #16920, .T. ) ;
#76=CARTESIAN_POINT ( 'NONE',  ( 19.18382676146983457, -4.683391092530263755, 11.49999999999998934 ) ) ;
#77=ADVANCED_FACE ( 'NONE', ( #5939 ), #75439, .F. ) ;
#78=B_SPLINE_CURVE_WITH_KNOTS ( 'NONE', 3,
 ( #65257, #57627, #41392, #64254 ),
 .UNSPECIFIED., .F., .F.,
 ( 4, 4 ),
 ( 0.2289244050901574346, 0.2299251521309229884 ),
 .UNSPECIFIED. ) ;
#79=AXIS2_PLACEMENT_3D ( 'NONE', #87672, #18153, #64361 ) ;
#82=CARTESIAN_POINT ( 'NONE',  ( -109.4089209358690056, -25.26578872481861993, 3.901360433916359671 ) ) ;
#84=VECTOR ( 'NONE', #37121, 1000.000000000000114 ) ;
#89=CARTESIAN_POINT ( 'NONE',  ( -41.52287095715006870, -23.47596703998600631, 11.44779298504229281 ) ) ;
#90=CARTESIAN_POINT ( 'NONE',  ( -66.52287095715006160, -24.64898659630528854, 1.056161002820824368 ) ) ;
#93=CARTESIAN_POINT ( 'NONE',  ( -61.52287095715008292, -24.51283580621364777, 0.6167428607019722619 ) ) ;
#94=CARTESIAN_POINT ( 'NONE',  ( -19.26508835251014773, 5.270845654819066084, 11.49999999999998934 ) ) ;
#95=EDGE_CURVE ( 'NONE', #59480, #61101, #43375, .T. ) ;
#96=CARTESIAN_POINT ( 'NONE',  ( -65.52287095715006160, -23.47596703998600631, 11.44779298504228748 ) ) ;
#97=CARTESIAN_POINT ( 'NONE',  ( -45.58890605949096653, -24.52399227489127043, 9.353111116836528183 ) ) ;
#98=ORIENTED_EDGE ( 'NONE', *, *, #94745, .T. ) ;
#99=EDGE_CURVE ( 'NONE', #55720, #33243, #52622, .T. ) ;
#100=EDGE_CURVE ( 'NONE', #61817, #96286, #13544, .T. ) ;
#101=CARTESIAN_POINT ( 'NONE',  ( -104.6228709571500133, -23.96177878511308634, 10.65340807706329684 ) ) ;
#102=CARTESIAN_POINT ( 'NONE',  ( -109.5174377349821953, -25.29012814469902182, 3.703579023877377807 ) ) ;
#103=CARTESIAN_POINT ( 'NONE',  ( -35.52193570048709148, -23.48783264082477729, -1.443836473390077479 ) ) ;
#104=CARTESIAN_POINT ( 'NONE',  ( -61.62287095715004881, -29.50247984919015209, -1.443849546365056913 ) ) ;
#107=CARTESIAN_POINT ( 'NONE',  ( -63.62287095715004881, -23.48786465467241058, 11.44779295918254824 ) ) ;
#108=LINE ( 'NONE', #99052, #42049 ) ;
#110=CARTESIAN_POINT ( 'NONE',  ( -6.888417027594036846, 19.07602104198033643, 11.49999999999998934 ) ) ;
#111=B_SPLINE_CURVE_WITH_KNOTS ( 'NONE', 3,
 ( #12004, #4406, #74405, #5887 ),
 .UNSPECIFIED., .F., .F.,
 ( 4, 4 ),
 ( 0.5701930854029353402, 0.5791995166750508739 ),
 .UNSPECIFIED. ) ;
#113=DIRECTION ( 'NONE',  ( -3.773278334453080206E-23, 0.9999999999976377785, 2.173523156925979975E-06 ) ) ;
#116=CARTESIAN_POINT ( 'NONE',  ( 17.11712468798820908, 10.61635618877791742, -1.500000000000002220 ) ) ;
#117=CARTESIAN_POINT ( 'NONE',  ( -19.68365937621761219, -7.520201837432793468, 11.49999999999999645 ) ) ;
#118=CARTESIAN_POINT ( 'NONE',  ( -16.97254739485517661, -14.18817111035334655, 11.49999999999998934 ) ) ;
#120=CARTESIAN_POINT ( 'NONE',  ( -17.34406541665444124, 10.97931167347951842, -1.500000000000002220 ) ) ;
#121=CARTESIAN_POINT ( 'NONE',  ( -95.51720277341769361, -23.85016227208581441, -0.8807180028928280890 ) ) ;
#124=CARTESIAN_POINT ( 'NONE',  ( -32.62287095715004881, -23.47593901973091235, -1.443836447539013301 ) ) ;
#125=VERTEX_POINT ( 'NONE', #61249 ) ;
#127=DIRECTION ( 'NONE',  ( -3.773278334453079618E-23, 0.9999999999976377785, 2.173523156925979975E-06 ) ) ;
#128=ORIENTED_EDGE ( 'NONE', *, *, #60112, .T. ) ;
#130=ORIENTED_EDGE ( 'NONE', *, *, #14486, .T. ) ;
#132=CARTESIAN_POINT ( 'NONE',  ( -71.62287095715005592, -23.72773821059536559, 11.05748984161097681 ) ) ;
#133=CARTESIAN_POINT ( 'NONE',  ( -68.53707658420209725, -24.66019654487199375, 8.947790411086122830 ) ) ;
#134=CARTESIAN_POINT ( 'NONE',  ( 13.18972694569024640, 15.87703813876158598, -1.500000000000002220 ) ) ;
#135=CARTESIAN_POINT ( 'NONE',  ( 1.064956243273112557, 21.61254047163424019, 11.49999999999999645 ) ) ;
#136=ORIENTED_EDGE ( 'NONE', *, *, #10032, .F. ) ;
#137=CARTESIAN_POINT ( 'NONE',  ( -83.62287095715005592, -24.64898659630528854, 1.056161002820826145 ) ) ;
#139=CARTESIAN_POINT ( 'NONE',  ( 1.438201247614206757, 22.34484416265529916, 11.49999999999998934 ) ) ;
#140=DIRECTION ( 'NONE',  ( -1.000000000000000000, -3.773278334444167608E-23, -8.201307833595939069E-29 ) ) ;
#141=DIRECTION ( 'NONE',  ( 0.000000000000000000, -2.173523156925979552E-06, 0.9999999999976378895 ) ) ;
#144=CARTESIAN_POINT ( 'NONE',  ( -49.59335215026359833, -24.15620529776627379, 10.23563542870661003 ) ) ;
#145=B_SPLINE_CURVE_WITH_KNOTS ( 'NONE', 3,
 ( #93012, #31119, #8793, #23489, #70690, #39734 ),
 .UNSPECIFIED., .F., .F.,
 ( 4, 2, 4 ),
 ( 0.000000000000000000, 0.001380764517853254455, 0.002761529035706508910 ),
 .UNSPECIFIED. ) ;
#146=VECTOR ( 'NONE', #42347, 1000.000000000000114 ) ;
#148=CARTESIAN_POINT ( 'NONE',  ( -15.06743543786183714, 14.52697759824333090, -1.500000000000002220 ) ) ;
#150=B_SPLINE_CURVE_WITH_KNOTS ( 'NONE', 3,
 ( #38455, #85628, #62820, #87130 ),
 .UNSPECIFIED., .F., .F.,
 ( 4, 4 ),
 ( 2.775557561562891351E-17, 0.0001000000000000167286 ),
 .UNSPECIFIED. ) ;
#151=B_SPLINE_CURVE_WITH_KNOTS ( 'NONE', 3,
 ( #689, #31133, #14407, #23004, #54988, #7294 ),
 .UNSPECIFIED., .F., .F.,
 ( 4, 2, 4 ),
 ( 3.593123586040311387E-14, 0.0002343744485612567175, 0.0004687488970865821619 ),
 .UNSPECIFIED. ) ;
#152=CARTESIAN_POINT ( 'NONE',  ( -69.62287095715005592, -29.50248528299804818, 1.056150453629036701 ) ) ;
#153=VERTEX_POINT ( 'NONE', #84561 ) ;
#154=CARTESIAN_POINT ( 'NONE',  ( -109.6330811136520111, -23.48786465467241769, 11.44779295918253759 ) ) ;
#155=CARTESIAN_POINT ( 'NONE',  ( 1.812468502196824760, -21.08352789287561180, -1.500000000000002220 ) ) ;
#157=CARTESIAN_POINT ( 'NONE',  ( -50.65003834120983583, -24.15503026093913164, -0.2815557561904566963 ) ) ;
#158=EDGE_CURVE ( 'NONE', #46090, #80749, #42232, .T. ) ;
#159=CARTESIAN_POINT ( 'NONE',  ( 14.98227958311676744, 15.82868232077399462, 11.49999999999998934 ) ) ;
#161=ADVANCED_FACE ( 'NONE', ( #15045 ), #7938, .F. ) ;
#163=CARTESIAN_POINT ( 'NONE',  ( -79.62287095715005592, -23.47593901973091235, -1.443836447539004642 ) ) ;
#164=CARTESIAN_POINT ( 'NONE',  ( 14.98227958311676744, 15.82868232077399462, -1.500000000000002220 ) ) ;
#165=CARTESIAN_POINT ( 'NONE',  ( -66.92287095715006728, -23.47593901973090169, -1.443836447538997536 ) ) ;
#166=ORIENTED_EDGE ( 'NONE', *, *, #99366, .F. ) ;
#170=EDGE_CURVE ( 'NONE', #72067, #41555, #93164, .T. ) ;
#172=ORIENTED_EDGE ( 'NONE', *, *, #47372, .F. ) ;
#173=EDGE_CURVE ( 'NONE', #72214, #47216, #85698, .T. ) ;
#175=DIRECTION ( 'NONE',  ( -1.000000000000000000, -3.773278334444166432E-23, -8.201307841325785021E-29 ) ) ;
#177=CARTESIAN_POINT ( 'NONE',  ( 4.903939382885006637, -20.63555827282145572, 11.49999999999998934 ) ) ;
#178=CARTESIAN_POINT ( 'NONE',  ( -80.35919894935766195, -25.30543142107805465, 4.505481316334992492 ) ) ;
#179=CARTESIAN_POINT ( 'NONE',  ( -79.38827465850120291, -25.03138204137674805, 7.124171970841336687 ) ) ;
#182=CARTESIAN_POINT ( 'NONE',  ( -4.359330469889163950, 18.88329184224734192, 11.49999999999998934 ) ) ;
#183=CARTESIAN_POINT ( 'NONE',  ( -39.97931365918082491, -25.30060000302003331, 6.009290021095885059 ) ) ;
#185=CARTESIAN_POINT ( 'NONE',  ( -14.34788840963776124, 13.16932220997287928, 11.49999999999999645 ) ) ;
#192=CARTESIAN_POINT ( 'NONE',  ( -64.62287095715005592, -23.47593901973091235, -1.443836447539007972 ) ) ;
#193=CARTESIAN_POINT ( 'NONE',  ( -101.2856530191658919, -25.24578106541012446, 3.795013565542035838 ) ) ;
#194=CARTESIAN_POINT ( 'NONE',  ( -18.74126595726828626, 5.813943427813767606, 11.49999999999998934 ) ) ;
#196=FACE_OUTER_BOUND ( 'NONE', #11738, .T. ) ;
#197=ORIENTED_EDGE ( 'NONE', *, *, #96086, .T. ) ;
#198=CARTESIAN_POINT ( 'NONE',  ( -19.30636564405121902, 9.640216152154000184, -1.500000000000002220 ) ) ;
#203=CARTESIAN_POINT ( 'NONE',  ( -13.16640216892762894, -18.94680327863774849, -1.500000000000002220 ) ) ;
#205=CARTESIAN_POINT ( 'NONE',  ( -93.51856585546278211, -23.73766607897670511, -1.055555164236453569 ) ) ;
#207=CARTESIAN_POINT ( 'NONE',  ( -113.5228709571500616, -29.50250786944525672, 11.44777988621622988 ) ) ;
#208=LINE ( 'NONE', #38761, #30674 ) ;
#209=CARTESIAN_POINT ( 'NONE',  ( -110.2723682709820565, -25.18516355925999406, 3.295595804301087117 ) ) ;
#210=CARTESIAN_POINT ( 'NONE',  ( -73.52287095715004739, -23.96177878511308990, 10.65340807706330217 ) ) ;
#211=CARTESIAN_POINT ( 'NONE',  ( -111.3738206124644279, -25.18425799667088327, 4.292346856177868375 ) ) ;
#212=CARTESIAN_POINT ( 'NONE',  ( 18.06118663784855372, 8.336529998961283994, 11.49999999999998934 ) ) ;
#214=CARTESIAN_POINT ( 'NONE',  ( 11.68167410197319001, -16.05257874518773065, -1.500000000000002220 ) ) ;
#216=EDGE_CURVE ( 'NONE', #67134, #36357, #40895, .T. ) ;
#218=AXIS2_PLACEMENT_3D ( 'NONE', #55658, #4225, #12317 ) ;
#219=CARTESIAN_POINT ( 'NONE',  ( -56.62287095715005592, -29.50250243563736774, 8.947779886222145151 ) ) ;
#221=CARTESIAN_POINT ( 'NONE',  ( -10.81534556030752725, -17.66751395530895152, 11.49999999999999645 ) ) ;
#225=CARTESIAN_POINT ( 'NONE',  ( 16.48639501038195121, -15.69157857782056276, 11.49999999999999645 ) ) ;
#227=CARTESIAN_POINT ( 'NONE',  ( -58.52287095715006160, -24.65952944569304250, 1.056160979905695463 ) ) ;
#228=CARTESIAN_POINT ( 'NONE',  ( -106.6228709571500559, -24.64898659630368627, 1.056161002820831474 ) ) ;
#229=B_SPLINE_CURVE_WITH_KNOTS ( 'NONE', 3,
 ( #25806, #12065, #89208, #96813 ),
 .UNSPECIFIED., .F., .F.,
 ( 4, 4 ),
 ( 0.000000000000000000, 0.0001000000000000028644 ),
 .UNSPECIFIED. ) ;
#230=ORIENTED_EDGE ( 'NONE', *, *, #33610, .F. ) ;
#231=CARTESIAN_POINT ( 'NONE',  ( 5.087728227403598424, 19.53446797131710611, 11.49999999999998934 ) ) ;
#232=CARTESIAN_POINT ( 'NONE',  ( -108.6228709571500275, -24.33927499327853639, 9.819080762295818943 ) ) ;
#233=DIRECTION ( 'NONE',  ( -3.773278334453080206E-23, 0.9999999999976377785, 2.173523156925979975E-06 ) ) ;
#234=VERTEX_POINT ( 'NONE', #92668 ) ;
#235=EDGE_LOOP ( 'NONE', ( #88022, #66563, #60750, #15385 ) ) ;
#236=DIRECTION ( 'NONE',  ( 0.000000000000000000, 0.9999999999976377785, 2.173523156925979975E-06 ) ) ;
#237=CARTESIAN_POINT ( 'NONE',  ( -19.55383134093860420, 11.88776249338449986, 11.49999999999998934 ) ) ;
#238=CARTESIAN_POINT ( 'NONE',  ( -51.23509499458276650, -25.18439743769400252, 3.726222305450818784 ) ) ;
#239=CARTESIAN_POINT ( 'NONE',  ( -20.67203406374276398, -6.343553224398504220, -1.500000000000002220 ) ) ;
#241=CARTESIAN_POINT ( 'NONE',  ( 4.013313563623547964, -20.52093592976233438, 11.49999999999999645 ) ) ;
#243=CARTESIAN_POINT ( 'NONE',  ( -124.5206819125863262, -24.15543982623907482, -0.2315651400026562945 ) ) ;
#244=CARTESIAN_POINT ( 'NONE',  ( -18.71521858236628333, -11.60751834597489740, 11.49999999999998934 ) ) ;
#246=CARTESIAN_POINT ( 'NONE',  ( -30.47287095715008576, -24.05150381395742443, 10.46526688926917181 ) ) ;
#247=ORIENTED_EDGE ( 'NONE', *, *, #73065, .T. ) ;
#248=AXIS2_PLACEMENT_3D ( 'NONE', #29119, #5785, #36741 ) ;
#252=DIRECTION ( 'NONE',  ( -1.000000000000000000, -3.773278334444167608E-23, -8.201307833595939069E-29 ) ) ;
#254=ORIENTED_EDGE ( 'NONE', *, *, #68054, .T. ) ;
#255=CARTESIAN_POINT ( 'NONE',  ( -61.64687923781918499, -25.15699314367416051, 3.101158825156976384 ) ) ;
#256=CARTESIAN_POINT ( 'NONE',  ( -101.5300974081266787, -25.27404751924990123, 3.391562929131038295 ) ) ;
#257=CARTESIAN_POINT ( 'NONE',  ( -36.47913385759269289, -24.65952944569304606, 1.056160979905694353 ) ) ;
#258=CARTESIAN_POINT ( 'NONE',  ( 20.32696876622996029, 2.630761579057304900, -1.500000000000002220 ) ) ;
#260=CARTESIAN_POINT ( 'NONE',  ( -99.47179591409185662, -25.28893848418214674, 5.641873549842387980 ) ) ;
#261=CARTESIAN_POINT ( 'NONE',  ( -44.54012218498173326, -24.34968618360933590, 0.1864209137778786995 ) ) ;
#263=CARTESIAN_POINT ( 'NONE',  ( 20.12748746789148413, 9.599020362109589755, -1.500000000000002220 ) ) ;
#267=B_SPLINE_CURVE_WITH_KNOTS ( 'NONE', 3,
 ( #48600, #903, #40970, #18128 ),
 .UNSPECIFIED., .F., .F.,
 ( 4, 4 ),
 ( 0.000000000000000000, 9.999999999998900014E-05 ),
 .UNSPECIFIED. ) ;
#269=CARTESIAN_POINT ( 'NONE',  ( -29.01900995608618317, -25.26247959377253238, 7.711473047842090978 ) ) ;
#270=CARTESIAN_POINT ( 'NONE',  ( -11.07951500695464553, -17.62175104703424466, 11.49999999999998934 ) ) ;
#272=ORIENTED_EDGE ( 'NONE', *, *, #40497, .T. ) ;
#273=CARTESIAN_POINT ( 'NONE',  ( -54.62287095715005592, -23.72747288104441665, -1.053458166803663776 ) ) ;
#274=EDGE_LOOP ( 'NONE', ( #98900, #37261, #35431, #93188 ) ) ;
#275=CARTESIAN_POINT ( 'NONE',  ( -51.52241826985714113, -25.12217690167820550, 6.308159032981181191 ) ) ;
#276=CARTESIAN_POINT ( 'NONE',  ( -20.98013922110768448, -1.350454208470041273, -1.500000000000002220 ) ) ;
#277=ORIENTED_EDGE ( 'NONE', *, *, #15628, .T. ) ;
#278=CARTESIAN_POINT ( 'NONE',  ( -69.52287095715006160, -23.96177878511308634, 10.65340807706329862 ) ) ;
#280=EDGE_CURVE ( 'NONE', #84354, #30802, #77932, .T. ) ;
#283=CARTESIAN_POINT ( 'NONE',  ( -92.63100859344015703, -24.15620529776628445, 10.23563542870660292 ) ) ;
#285=CARTESIAN_POINT ( 'NONE',  ( 21.60277357391871433, -5.133695162202882578, 11.49999999999999645 ) ) ;
#286=ORIENTED_EDGE ( 'NONE', *, *, #56606, .F. ) ;
#291=CARTESIAN_POINT ( 'NONE',  ( 20.84710439121840864, 8.857176948214046774, 11.49999999999998934 ) ) ;
#293=CARTESIAN_POINT ( 'NONE',  ( -28.87481646230549615, -25.02372474006351410, 6.909395630504118202 ) ) ;
#294=VERTEX_POINT ( 'NONE', #62753 ) ;
#295=B_SPLINE_CURVE_WITH_KNOTS ( 'NONE', 3,
 ( #30244, #17024, #22619, #37869 ),
 .UNSPECIFIED., .F., .F.,
 ( 4, 4 ),
 ( 0.6892680438423023359, 0.6902687908830678065 ),
 .UNSPECIFIED. ) ;
#298=ORIENTED_EDGE ( 'NONE', *, *, #47645, .F. ) ;
#300=EDGE_CURVE ( 'NONE', #37450, #64205, #96659, .T. ) ;
#302=CARTESIAN_POINT ( 'NONE',  ( -19.13055903301823335, -6.388282315271819556, -1.500000000000002220 ) ) ;
#303=CARTESIAN_POINT ( 'NONE',  ( -81.62287095715004170, -24.66019654487199020, 8.947790411086131712 ) ) ;
#305=FACE_OUTER_BOUND ( 'NONE', #66048, .T. ) ;
#306=CARTESIAN_POINT ( 'NONE',  ( -11.14805103425725719, -19.39388463112642214, -1.500000000000002220 ) ) ;
#309=CARTESIAN_POINT ( 'NONE',  ( -101.3040450898205620, -25.16257414492327626, 6.746837491236538753 ) ) ;
#310=DIRECTION ( 'NONE',  ( 3.773278334444166432E-23, -1.000000000000000000, 0.000000000000000000 ) ) ;
#314=CARTESIAN_POINT ( 'NONE',  ( -130.5728709571500588, -24.04615231314292245, -0.4716817114508914388 ) ) ;
#315=CARTESIAN_POINT ( 'NONE',  ( -9.627943313441900131, 16.98966435471970726, 11.49999999999998934 ) ) ;
#317=CARTESIAN_POINT ( 'NONE',  ( 17.49997855696484095, 12.48231381050728928, -1.500000000000002220 ) ) ;
#318=CARTESIAN_POINT ( 'NONE',  ( -128.5901389850763508, -23.73766607897672287, -1.055555164236423149 ) ) ;
#319=CARTESIAN_POINT ( 'NONE',  ( -121.5228709571500332, -23.73907113216989728, -1.053371485793244355 ) ) ;
#321=CARTESIAN_POINT ( 'NONE',  ( -80.62287095715004170, -23.84081130438200802, 10.88220057463249546 ) ) ;
#322=CARTESIAN_POINT ( 'NONE',  ( 4.181975289622855918, -22.47981636197143374, -1.500000000000002220 ) ) ;
#325=CARTESIAN_POINT ( 'NONE',  ( -96.59678146177949998, -23.73791477778911840, 11.05961554403170410 ) ) ;
#326=CARTESIAN_POINT ( 'NONE',  ( -92.62287095715007013, -23.94994826722565762, -0.6494450866342730277 ) ) ;
#327=CARTESIAN_POINT ( 'NONE',  ( -12.91570554291229023, -15.35452705144416896, 11.49999999999999645 ) ) ;
#328=CARTESIAN_POINT ( 'NONE',  ( -79.92757955003747838, -25.31594328122231730, 4.561565462960619932 ) ) ;
#331=CARTESIAN_POINT ( 'NONE',  ( -115.6228709571500559, -29.50248789122583659, 2.256150453626215580 ) ) ;
#332=ORIENTED_EDGE ( 'NONE', *, *, #93875, .T. ) ;
#333=CARTESIAN_POINT ( 'NONE',  ( -85.62287095715005592, -23.47593901973091235, -1.443836447539002865 ) ) ;
#334=CARTESIAN_POINT ( 'NONE',  ( -109.9631709994365423, -25.11668225391187548, 2.867640993816269912 ) ) ;
#335=CARTESIAN_POINT ( 'NONE',  ( -3.058130702743298901, -21.54894043062209263, 11.49999999999998934 ) ) ;
#336=CARTESIAN_POINT ( 'NONE',  ( -45.52287095715009002, -24.52323809116982645, 9.355190652339423707 ) ) ;
#337=CARTESIAN_POINT ( 'NONE',  ( -3.719764837209879271, -19.30396570740023421, -1.500000000000002220 ) ) ;
#339=CARTESIAN_POINT ( 'NONE',  ( -97.52287095715006160, -29.50248528299804818, 1.056150453629042030 ) ) ;
#341=CARTESIAN_POINT ( 'NONE',  ( -38.55620429048340014, -23.47596703998600276, 11.44779298504227505 ) ) ;
#343=CARTESIAN_POINT ( 'NONE',  ( -20.56140336115741718, 0.6910293267889283664, 11.49999999999999645 ) ) ;
#345=AXIS2_PLACEMENT_3D ( 'NONE', #4716, #83319, #98039 ) ;
#346=CARTESIAN_POINT ( 'NONE',  ( -120.5530855258607659, -24.73486907724918638, 1.287355809206965684 ) ) ;
#347=EDGE_LOOP ( 'NONE', ( #79694, #28906, #10200, #93002 ) ) ;
#348=EDGE_CURVE ( 'NONE', #76528, #58306, #14323, .T. ) ;
#349=CARTESIAN_POINT ( 'NONE',  ( -99.52764846858842418, -25.31296290679074090, 3.999772165348554509 ) ) ;
#350=CARTESIAN_POINT ( 'NONE',  ( -39.56145255469812128, -25.28892524838338929, 3.766659524289464045 ) ) ;
#351=CARTESIAN_POINT ( 'NONE',  ( -78.52287095715006160, -24.65952944569304606, 1.056160979905698794 ) ) ;
#352=CARTESIAN_POINT ( 'NONE',  ( -90.62287095715004170, -29.50247984919015209, -1.443849546365051806 ) ) ;
#353=EDGE_CURVE ( 'NONE', #31349, #84710, #49410, .T. ) ;
#354=CARTESIAN_POINT ( 'NONE',  ( -25.96779814532654385, -24.61459876899060362, 7.161766614681138066 ) ) ;
#355=CARTESIAN_POINT ( 'NONE',  ( -42.62287095715004881, -23.72773821059535848, 11.05748984161097503 ) ) ;
#357=CARTESIAN_POINT ( 'NONE',  ( 19.36532470938277228, 12.59445105952145738, 11.49999999999999645 ) ) ;
#358=CARTESIAN_POINT ( 'NONE',  ( 21.74077840044056842, -6.890983112422549794, -1.500000000000002220 ) ) ;
#359=CARTESIAN_POINT ( 'NONE',  ( -74.58800651555678485, -24.34968618360933945, 0.1864209137778816139 ) ) ;
#360=CARTESIAN_POINT ( 'NONE',  ( -75.52287095715007581, -23.47596703998600631, 11.44779298504228571 ) ) ;
#361=CARTESIAN_POINT ( 'NONE',  ( -86.52287095715006160, -24.64965694238575011, 8.947790433994196491 ) ) ;
#363=CARTESIAN_POINT ( 'NONE',  ( 20.99545381566289137, 7.807860396396394620, 11.49999999999999645 ) ) ;
#364=EDGE_LOOP ( 'NONE', ( #5040, #85322, #20289, #51409 ) ) ;
#366=CARTESIAN_POINT ( 'NONE',  ( -38.62287095715006302, -24.33927499327853994, 9.819080762295817166 ) ) ;
#367=CARTESIAN_POINT ( 'NONE',  ( 20.11839708684271244, 8.774209887332036217, 11.49999999999998934 ) ) ;
#370=CARTESIAN_POINT ( 'NONE',  ( -44.57673106130640406, -24.66019654487199375, 8.947790411086115725 ) ) ;
#371=CARTESIAN_POINT ( 'NONE',  ( -68.94601647182436466, -25.22897554200561387, 6.368117921112105506 ) ) ;
#372=ORIENTED_EDGE ( 'NONE', *, *, #92617, .T. ) ;
#373=CARTESIAN_POINT ( 'NONE',  ( -48.98775370671620522, -25.18486450346212990, 6.713331287310639439 ) ) ;
#374=CARTESIAN_POINT ( 'NONE',  ( -96.62287095715005592, -23.47593901973091235, -1.443836447539001089 ) ) ;
#375=ORIENTED_EDGE ( 'NONE', *, *, #50984, .T. ) ;
#376=CARTESIAN_POINT ( 'NONE',  ( 4.362881659454829197, 20.01674633476859810, -1.500000000000002220 ) ) ;
#378=ORIENTED_EDGE ( 'NONE', *, *, #89968, .F. ) ;
#379=ORIENTED_EDGE ( 'NONE', *, *, #40213, .F. ) ;
#380=EDGE_LOOP ( 'NONE', ( #36956, #93992, #32879, #72303 ) ) ;
#381=CARTESIAN_POINT ( 'NONE',  ( -17.29220519630379016, 15.29500218549028645, -1.500000000000002220 ) ) ;
#382=CARTESIAN_POINT ( 'NONE',  ( -49.11363384361381890, -25.26016026082141508, 3.839858232430332308 ) ) ;
#383=CARTESIAN_POINT ( 'NONE',  ( 13.49383759531269433, -15.17088004136028090, -1.500000000000002220 ) ) ;
#384=EDGE_LOOP ( 'NONE', ( #413, #73949, #56206, #45383 ) ) ;
#385=DIRECTION ( 'NONE',  ( -3.773278334444167608E-23, 1.000000000000000000, 0.000000000000000000 ) ) ;
#387=B_SPLINE_CURVE_WITH_KNOTS ( 'NONE', 3,
 ( #75454, #7448, #84075, #77452, #61762, #29795 ),
 .UNSPECIFIED., .F., .F.,
 ( 4, 2, 4 ),
 ( 0.000000000000000000, 0.001380901958385387027, 0.002761803916770774053 ),
 .UNSPECIFIED. ) ;
#388=CARTESIAN_POINT ( 'NONE',  ( -47.62287095715004881, -23.48783264082478084, -1.443836473390070596 ) ) ;
#389=CARTESIAN_POINT ( 'NONE',  ( -70.53622126975956519, -24.83618233451450052, 1.606449574219541487 ) ) ;
#390=CARTESIAN_POINT ( 'NONE',  ( -19.99255411920323056, 7.849732829375159149, 11.49999999999999645 ) ) ;
#395=CARTESIAN_POINT ( 'NONE',  ( 14.61947915221463923, 14.71393552341326760, -1.500000000000002220 ) ) ;
#398=ORIENTED_EDGE ( 'NONE', *, *, #80161, .T. ) ;
#400=B_SPLINE_SURFACE_WITH_KNOTS ( 'NONE', 3, 3, ( 
 ( #90759, #84138, #13620, #97377 ),
 ( #20238, #51206, #1425, #69923 ),
 ( #7519, #31361, #38474, #24247 ),
 ( #55220, #22724, #15629, #916 ),
 ( #54714, #47601, #100343, #77019 ),
 ( #86148, #39973, #7021, #31868 ),
 ( #32361, #93755, #84641, #46094 ) ),
 .UNSPECIFIED., .F., .F., .F.,
 ( 4, 3, 4 ),
 ( 4, 4 ),
 ( 0.7945040050992240310, 0.8970133687736498995, 0.9995227324480757680 ),
 ( 0.4095980817935837015, 0.4107999040036969807 ),
 .UNSPECIFIED. ) ;
#401=CARTESIAN_POINT ( 'NONE',  ( -111.5891399377753004, -24.35071581493544457, 9.817618358456018157 ) ) ;
#402=CARTESIAN_POINT ( 'NONE',  ( -129.5228709571500758, -23.47596703998600631, 11.44779298504227683 ) ) ;
#403=ORIENTED_EDGE ( 'NONE', *, *, #6348, .T. ) ;
#407=CARTESIAN_POINT ( 'NONE',  ( -65.63576524279528712, -24.52300882791528380, 0.6510814631126250474 ) ) ;
#408=CARTESIAN_POINT ( 'NONE',  ( 21.96865551644221881, -1.217672407684077918, 11.49999999999999645 ) ) ;
#410=CARTESIAN_POINT ( 'NONE',  ( -1.585881643086899606, 22.48459252949185228, 11.49999999999998934 ) ) ;
#411=CARTESIAN_POINT ( 'NONE',  ( -1.027814097295878693, -20.98676634966329146, 11.49999999999998934 ) ) ;
#413=ORIENTED_EDGE ( 'NONE', *, *, #99246, .F. ) ;
#414=VECTOR ( 'NONE', #39030, 1000.000000000000114 ) ;
#416=ORIENTED_EDGE ( 'NONE', *, *, #89969, .T. ) ;
#419=DIRECTION ( 'NONE',  ( -3.773278334453079030E-23, 0.9999999999976377785, 2.173523156925979128E-06 ) ) ;
#420=VERTEX_POINT ( 'NONE', #73844 ) ;
#421=CARTESIAN_POINT ( 'NONE',  ( 19.82261944725993175, 7.364942908566579405, -1.500000000000002220 ) ) ;
#422=CARTESIAN_POINT ( 'NONE',  ( -99.62287095715005592, -23.48786465467241769, 11.44779295918254114 ) ) ;
#423=CARTESIAN_POINT ( 'NONE',  ( -50.75822869421170225, -25.26041111912611115, 7.539272917437609856 ) ) ;
#424=CARTESIAN_POINT ( 'NONE',  ( -121.6252488971726677, -24.15543982623907482, -0.2315651400026574047 ) ) ;
#425=CARTESIAN_POINT ( 'NONE',  ( -79.52287095715006160, -24.64898659630367916, 1.056161002820826145 ) ) ;
#426=CARTESIAN_POINT ( 'NONE',  ( -127.5228709571500616, -23.48786465467242479, 11.44779295918253581 ) ) ;
#427=CARTESIAN_POINT ( 'NONE',  ( 15.99899278244174639, -15.33069297701436184, -1.500000000000002220 ) ) ;
#428=CARTESIAN_POINT ( 'NONE',  ( -71.51636566736119960, -23.73766607897670156, -1.055555164236456012 ) ) ;
#433=CARTESIAN_POINT ( 'NONE',  ( -126.5893519502692754, -24.51314013834316796, 0.6176544820404223923 ) ) ;
#434=CARTESIAN_POINT ( 'NONE',  ( -100.6255027387640979, -24.83618233451450763, 1.606449574219537713 ) ) ;
#437=CARTESIAN_POINT ( 'NONE',  ( 8.422564666779264186, -17.53554878399664574, 11.49999999999998934 ) ) ;
#439=CARTESIAN_POINT ( 'NONE',  ( -12.70309173801008562, -17.24390854791867511, -1.500000000000002220 ) ) ;
#440=CARTESIAN_POINT ( 'NONE',  ( -62.55373037630388211, -23.96119346886881019, -0.6495511937832096905 ) ) ;
#441=CARTESIAN_POINT ( 'NONE',  ( -60.65501803048972107, -23.85049219812968602, 10.88485053497088728 ) ) ;
#442=CARTESIAN_POINT ( 'NONE',  ( -51.53639160008312103, -24.51314013834315730, 0.6176544820404109570 ) ) ;
#443=CARTESIAN_POINT ( 'NONE',  ( -100.7282901814618583, -25.27359982393476656, 3.329829818474457692 ) ) ;
#444=CARTESIAN_POINT ( 'NONE',  ( -0.6305239314742796530, -22.70799625201654592, -1.500000000000002220 ) ) ;
#445=CARTESIAN_POINT ( 'NONE',  ( -98.63223275675622403, -23.96119346886881019, -0.6495511937832081362 ) ) ;
#447=CARTESIAN_POINT ( 'NONE',  ( -19.70454523906213495, -2.556213046838741842, 11.49999999999999645 ) ) ;
#450=CARTESIAN_POINT ( 'NONE',  ( -38.62287095715005592, -29.50250786944525672, 11.44777988621624232 ) ) ;
#453=CARTESIAN_POINT ( 'NONE',  ( -80.52287095715006160, -24.99156044556202616, 7.747789690856173195 ) ) ;
#455=CARTESIAN_POINT ( 'NONE',  ( 21.64940796807912449, -0.2623997510114038922, -1.500000000000002220 ) ) ;
#456=CARTESIAN_POINT ( 'NONE',  ( -29.62287095715004881, -23.64926103841893124, 11.05761042169888597 ) ) ;
#457=CARTESIAN_POINT ( 'NONE',  ( -19.27395093635484713, 2.380100695660296140, -1.500000000000002220 ) ) ;
#458=CARTESIAN_POINT ( 'NONE',  ( -55.58285685940607834, -24.73531770709094957, 8.716586749053510275 ) ) ;
#459=CARTESIAN_POINT ( 'NONE',  ( 4.164567180745167185, 19.39263604865329071, 11.49999999999998934 ) ) ;
#461=ORIENTED_EDGE ( 'NONE', *, *, #57251, .T. ) ;
#462=CARTESIAN_POINT ( 'NONE',  ( -17.59887021274124663, -10.25344800880639262, 11.49999999999999645 ) ) ;
#463=LINE ( 'NONE', #45650, #65151 ) ;
#464=EDGE_CURVE ( 'NONE', #42504, #27734, #71857, .T. ) ;
#466=AXIS2_PLACEMENT_3D ( 'NONE', #79939, #73829, #3833 ) ;
#467=ORIENTED_EDGE ( 'NONE', *, *, #43495, .T. ) ;
#468=B_SPLINE_CURVE_WITH_KNOTS ( 'NONE', 3,
 ( #83772, #68559, #83277, #53344, #90893, #52341 ),
 .UNSPECIFIED., .F., .F.,
 ( 4, 2, 4 ),
 ( 0.000000000000000000, 0.001380901958385393966, 0.002761803916770787931 ),
 .UNSPECIFIED. ) ;
#469=CARTESIAN_POINT ( 'NONE',  ( -30.64427850938830744, -23.56000036390796026, 11.50200000000000600 ) ) ;
#470=CARTESIAN_POINT ( 'NONE',  ( -111.3776484685884469, -25.29712067403330877, 4.332404411321261861 ) ) ;
#471=CARTESIAN_POINT ( 'NONE',  ( -48.90136019426822145, -25.25214628733238342, 5.866402775706137440 ) ) ;
#474=CARTESIAN_POINT ( 'NONE',  ( 19.67429046578372365, -4.105084037421226739, -1.500000000000002220 ) ) ;
#476=AXIS2_PLACEMENT_3D ( 'NONE', #41465, #33338, #88143 ) ;
#477=VERTEX_POINT ( 'NONE', #49023 ) ;
#478=CARTESIAN_POINT ( 'NONE',  ( -107.6228709571500701, -23.48786465467241769, 11.44779295918253936 ) ) ;
#479=CARTESIAN_POINT ( 'NONE',  ( 1.119804705421552748, 22.86502198858056545, 11.49999999999999645 ) ) ;
#480=CARTESIAN_POINT ( 'NONE',  ( -10.65177407370799045, -20.06881281718593613, 11.49999999999998934 ) ) ;
#481=EDGE_LOOP ( 'NONE', ( #19965, #25245, #83249, #77513 ) ) ;
#482=CARTESIAN_POINT ( 'NONE',  ( -71.70841769935766763, -25.25720466352798255, 6.192981421160952848 ) ) ;
#484=DIRECTION ( 'NONE',  ( 0.000000000000000000, -0.9999999999976377785, -2.173523156925979975E-06 ) ) ;
#485=CARTESIAN_POINT ( 'NONE',  ( -38.58688038665032138, -24.35071581493542325, 9.817618358456030592 ) ) ;
#486=DIRECTION ( 'NONE',  ( 0.000000000000000000, 0.9999999999976377785, 2.173523156925979975E-06 ) ) ;
#487=EDGE_CURVE ( 'NONE', #56501, #14750, #63985, .T. ) ;
#489=CARTESIAN_POINT ( 'NONE',  ( -128.5559268670633628, -23.96169478059714919, 10.65365249895717170 ) ) ;
#491=EDGE_LOOP ( 'NONE', ( #43848, #52174, #5109, #74657 ) ) ;
#492=CARTESIAN_POINT ( 'NONE',  ( 19.91419669613914678, 4.404666692190684962, 11.49999999999998934 ) ) ;
#493=ORIENTED_EDGE ( 'NONE', *, *, #85072, .F. ) ;
#494=CARTESIAN_POINT ( 'NONE',  ( -18.50152239663938403, 13.63810111590111163, 11.49999999999998934 ) ) ;
#495=CARTESIAN_POINT ( 'NONE',  ( -54.50227307414417766, -24.15620529776628089, 10.23563542870661180 ) ) ;
#498=CARTESIAN_POINT ( 'NONE',  ( -108.5134006316627051, -24.51419770103157347, 9.386484678747168076 ) ) ;
#499=CARTESIAN_POINT ( 'NONE',  ( -80.77625289099501060, -25.13967656840255671, 7.064051687917259237 ) ) ;
#500=VECTOR ( 'NONE', #98403, 1000.000000000000114 ) ;
#501=CARTESIAN_POINT ( 'NONE',  ( -111.5228709571500616, -23.47596703998600631, 11.44779298504228038 ) ) ;
#502=CARTESIAN_POINT ( 'NONE',  ( 19.59546714036918758, 8.467717511154198462, 11.49999999999999645 ) ) ;
#503=VERTEX_POINT ( 'NONE', #81467 ) ;
#506=CARTESIAN_POINT ( 'NONE',  ( -2.516727866726558460, 22.04588476715296963, -1.500000000000002220 ) ) ;
#507=CARTESIAN_POINT ( 'NONE',  ( 6.115004186001010922, -19.73231167505474559, 11.49999999999998934 ) ) ;
#512=CARTESIAN_POINT ( 'NONE',  ( -109.8219511710470897, -25.27682916472742747, 5.738454893586274252 ) ) ;
#513=CARTESIAN_POINT ( 'NONE',  ( -69.85667726116794540, -25.25978459231412288, 3.590539514744167437 ) ) ;
#514=ORIENTED_EDGE ( 'NONE', *, *, #94702, .T. ) ;
#515=CARTESIAN_POINT ( 'NONE',  ( -91.51496719381653122, -23.96119346886880663, -0.6495511937832073590 ) ) ;
#516=ORIENTED_EDGE ( 'NONE', *, *, #47148, .F. ) ;
#518=CARTESIAN_POINT ( 'NONE',  ( -58.65647576671169361, -23.48786465467241058, 11.44779295918254824 ) ) ;
#519=B_SPLINE_CURVE_WITH_KNOTS ( 'NONE', 3,
 ( #29528, #59008, #59497, #60009 ),
 .UNSPECIFIED., .F., .F.,
 ( 4, 4 ),
 ( 0.000000000000000000, 9.999999999999592548E-05 ),
 .UNSPECIFIED. ) ;
#520=CARTESIAN_POINT ( 'NONE',  ( -72.62287095715005592, -29.50250786944525672, 11.44777988621623699 ) ) ;
#521=CARTESIAN_POINT ( 'NONE',  ( 20.60118427460899326, -2.865472796819775958, -1.500000000000002220 ) ) ;
#523=CARTESIAN_POINT ( 'NONE',  ( 21.44370820036873937, 4.193779532373530294, 11.49999999999999645 ) ) ;
#524=CARTESIAN_POINT ( 'NONE',  ( -36.52287095715006870, -23.47596703998600631, 11.44779298504229281 ) ) ;
#525=CARTESIAN_POINT ( 'NONE',  ( -100.0539824966801064, -25.04132515376273815, 7.523549795824772346 ) ) ;
#526=CARTESIAN_POINT ( 'NONE',  ( -22.07377061809603092, 4.253497373390751513, 11.49999999999998934 ) ) ;
#527=DIRECTION ( 'NONE',  ( 0.000000000000000000, 2.173523156925980399E-06, -0.9999999999976378895 ) ) ;
#528=DIRECTION ( 'NONE',  ( 0.000000000000000000, 2.173523156925980399E-06, -0.9999999999976378895 ) ) ;
#530=B_SPLINE_SURFACE_WITH_KNOTS ( 'NONE', 3, 3, ( 
 ( #12800, #88452, #89940, #49903 ),
 ( #43775, #66634, #74220, #34665 ),
 ( #5201, #18924, #97549, #50393 ),
 ( #28532, #11815, #19922, #44276 ),
 ( #73230, #59496, #20407, #74703 ),
 ( #28049, #59007, #65137, #96551 ),
 ( #89446, #36159, #5698, #12302 ) ),
 .UNSPECIFIED., .F., .F., .F.,
 ( 4, 3, 4 ),
 ( 4, 4 ),
 ( 0.0004766839783837975792, 0.1029713700210903304, 0.2054660560637968647 ),
 ( 0.8297050600404040077, 0.8311006089866127544 ),
 .UNSPECIFIED. ) ;
#535=B_SPLINE_CURVE_WITH_KNOTS ( 'NONE', 3,
 ( #98354, #82143, #12628, #12120 ),
 .UNSPECIFIED., .F., .F.,
 ( 4, 4 ),
 ( 0.000000000000000000, 9.999999999998897304E-05 ),
 .UNSPECIFIED. ) ;
#536=CARTESIAN_POINT ( 'NONE',  ( 9.714863677370791706, 19.00186346016302608, -1.500000000000002220 ) ) ;
#538=CARTESIAN_POINT ( 'NONE',  ( -19.68365937621761219, -7.520201837432793468, 11.49999999999998934 ) ) ;
#539=CARTESIAN_POINT ( 'NONE',  ( -30.49551068477055082, -24.38002254354092102, 0.3015907515355735202 ) ) ;
#540=CARTESIAN_POINT ( 'NONE',  ( 10.26108024787556516, -17.11367029881254709, -1.500000000000002220 ) ) ;
#541=CARTESIAN_POINT ( 'NONE',  ( -50.52448152296889106, -25.00182538069147142, 7.747789668545043362 ) ) ;
#542=CARTESIAN_POINT ( 'NONE',  ( -50.18441529348658747, -25.04472180003372728, 7.555573460512422734 ) ) ;
#543=CARTESIAN_POINT ( 'NONE',  ( 21.99661117994144988, 0.4758108284031232760, -1.500000000000002220 ) ) ;
#545=ORIENTED_EDGE ( 'NONE', *, *, #54619, .T. ) ;
#546=CARTESIAN_POINT ( 'NONE',  ( -30.64535876238280565, -23.53198925593397917, 11.48393099501408976 ) ) ;
#547=EDGE_CURVE ( 'NONE', #74034, #7838, #11942, .T. ) ;
#548=VECTOR ( 'NONE', #22485, 1000.000000000000114 ) ;
#549=CARTESIAN_POINT ( 'NONE',  ( -54.62287095715004170, -23.47596703998600631, 11.44779298504227505 ) ) ;
#550=CARTESIAN_POINT ( 'NONE',  ( -19.40898059523135544, 7.551958013340856368, 11.49999999999999645 ) ) ;
#551=ADVANCED_FACE ( 'NONE', ( #80960 ), #76509, .T. ) ;
#553=VECTOR ( 'NONE', #56652, 1000.000000000000114 ) ;
#555=PLANE ( 'NONE',  #88668 ) ;
#556=CARTESIAN_POINT ( 'NONE',  ( 20.93798385506118365, 3.901641247904229282, 11.49999999999998934 ) ) ;
#557=CARTESIAN_POINT ( 'NONE',  ( -29.58953762381671737, -24.57142930420317128, 8.947790468830323363 ) ) ;
#558=CARTESIAN_POINT ( 'NONE',  ( -54.62287095715005592, -23.47593901973091235, -1.443836447539009749 ) ) ;
#559=CARTESIAN_POINT ( 'NONE',  ( -61.52287095715006160, -23.47596703998600631, 11.44779298504228926 ) ) ;
#560=DIRECTION ( 'NONE',  ( 0.000000000000000000, -0.9999999999976377785, -2.173523156925979128E-06 ) ) ;
#561=CARTESIAN_POINT ( 'NONE',  ( -5.199590022849982063, -21.90925200621149571, -1.500000000000002220 ) ) ;
#562=CARTESIAN_POINT ( 'NONE',  ( -56.52287095715006870, -23.47596703998600631, 11.44779298504228926 ) ) ;
#565=CARTESIAN_POINT ( 'NONE',  ( 7.987771016649366729, -18.01272016045900415, 11.49999999999999645 ) ) ;
#566=LINE ( 'NONE', #91908, #14699 ) ;
#569=CARTESIAN_POINT ( 'NONE',  ( -123.6228709571500559, -24.65952944569304961, 1.056160979905703234 ) ) ;
#570=LINE ( 'NONE', #31018, #59416 ) ;
#571=CARTESIAN_POINT ( 'NONE',  ( -100.3128489789178559, -25.25095783679409323, 5.229225670637348777 ) ) ;
#575=CARTESIAN_POINT ( 'NONE',  ( 12.99534586470982234, -14.87506298573330632, 11.49999999999998934 ) ) ;
#577=CARTESIAN_POINT ( 'NONE',  ( -109.7483548522739056, -25.21846411683590716, 3.465899786825440643 ) ) ;
#578=VECTOR ( 'NONE', #51125, 1000.000000000000114 ) ;
#582=CARTESIAN_POINT ( 'NONE',  ( -124.5228709571500758, -23.95044443724993144, 10.65354141964648882 ) ) ;
#583=PLANE ( 'NONE',  #76593 ) ;
#584=CARTESIAN_POINT ( 'NONE',  ( -65.62287095715005592, -23.48786465467241058, 11.44779295918254647 ) ) ;
#585=CARTESIAN_POINT ( 'NONE',  ( -99.20586904084365187, -25.26638419840477923, 7.003176680450737379 ) ) ;
#588=AXIS2_PLACEMENT_3D ( 'NONE', #34020, #81693, #56876 ) ;
#589=CARTESIAN_POINT ( 'NONE',  ( -124.5228709571500616, -24.65952944569305316, 1.056160979905705899 ) ) ;
#590=CARTESIAN_POINT ( 'NONE',  ( -16.75416981316412190, 10.96944243606782443, 11.49999999999998934 ) ) ;
#592=DIRECTION ( 'NONE',  ( -3.773278334453079030E-23, 0.9999999999976377785, 2.173523156925979128E-06 ) ) ;
#593=ORIENTED_EDGE ( 'NONE', *, *, #9471, .T. ) ;
#594=CARTESIAN_POINT ( 'NONE',  ( -56.62287095715005592, -29.50247984919015209, -1.443849546365056913 ) ) ;
#595=CARTESIAN_POINT ( 'NONE',  ( -73.55620429048340725, -23.47596703998600276, 11.44779298504227683 ) ) ;
#596=CARTESIAN_POINT ( 'NONE',  ( -120.6228709571500701, -25.00158670708909625, 2.256160236439166411 ) ) ;
#597=CARTESIAN_POINT ( 'NONE',  ( -82.55620429048339304, -24.64965694238575011, 8.947790433994194714 ) ) ;
#600=ADVANCED_FACE ( 'NONE', ( #28667 ), #59629, .T. ) ;
#601=B_SPLINE_SURFACE_WITH_KNOTS ( 'NONE', 3, 3, ( 
 ( #8281, #91510, #21989, #83905 ),
 ( #45359, #37730, #99610, #3190 ),
 ( #17899, #80295, #25507, #32618 ),
 ( #86404, #64098, #23997, #54966 ),
 ( #40733, #10788, #71692, #86901 ),
 ( #56977, #17393, #95016, #41752 ),
 ( #33623, #16383, #33120, #56480 ),
 ( #47349, #16889, #87404, #94515 ),
 ( #78273, #1679, #8784, #39722 ),
 ( #55974, #49366, #64605, #63593 ) ),
 .UNSPECIFIED., .F., .F., .F.,
 ( 4, 3, 3, 4 ),
 ( 4, 4 ),
 ( 0.7022005934544808259, 0.7765311282028796169, 0.8508616629512784080, 0.9995227324480761011 ),
 ( 0.4495482509261787829, 0.4508289003306459319 ),
 .UNSPECIFIED. ) ;
#603=EDGE_CURVE ( 'NONE', #68323, #2429, #30152, .T. ) ;
#605=ORIENTED_EDGE ( 'NONE', *, *, #96875, .F. ) ;
#606=B_SPLINE_CURVE_WITH_KNOTS ( 'NONE', 3,
 ( #65863, #97282, #4446, #35397 ),
 .UNSPECIFIED., .F., .F.,
 ( 4, 4 ),
 ( 0.3500358765290026430, 0.3590423078011182323 ),
 .UNSPECIFIED. ) ;
#608=CARTESIAN_POINT ( 'NONE',  ( 9.679018533540549640, -17.85022214266596308, -1.500000000000002220 ) ) ;
#609=CARTESIAN_POINT ( 'NONE',  ( -115.5228709571500474, -23.47593901973090524, -1.443836447538996204 ) ) ;
#611=ADVANCED_FACE ( 'NONE', ( #5824 ), #44904, .F. ) ;
#612=CARTESIAN_POINT ( 'NONE',  ( -127.6228709571500275, -23.48786465467242124, 11.44779295918253403 ) ) ;
#614=ORIENTED_EDGE ( 'NONE', *, *, #19902, .T. ) ;
#615=CARTESIAN_POINT ( 'NONE',  ( -114.5228709571500616, -29.50250786944525672, 11.44777988621622988 ) ) ;
#616=CARTESIAN_POINT ( 'NONE',  ( -17.82723130383223165, -9.322377578706960932, -1.500000000000002220 ) ) ;
#617=AXIS2_PLACEMENT_3D ( 'NONE', #79498, #95727, #71902 ) ;
#618=CARTESIAN_POINT ( 'NONE',  ( 19.82261944725993175, 7.364942908566579405, 11.49999999999999645 ) ) ;
#620=CARTESIAN_POINT ( 'NONE',  ( -21.51168160490077952, -5.175097382202364926, -1.500000000000002220 ) ) ;
#621=CARTESIAN_POINT ( 'NONE',  ( -10.41206725544052780, -17.73373708237225799, -1.500000000000002220 ) ) ;
#622=CARTESIAN_POINT ( 'NONE',  ( -60.55976763516859052, -23.85016227208580375, -0.8807180028928355275 ) ) ;
#623=VERTEX_POINT ( 'NONE', #90068 ) ;
#624=CARTESIAN_POINT ( 'NONE',  ( -94.52287095715003318, -24.66019654487199730, 8.947790411086124607 ) ) ;
#625=ORIENTED_EDGE ( 'NONE', *, *, #15400, .T. ) ;
#626=CARTESIAN_POINT ( 'NONE',  ( -85.62287095715004170, -23.85229601348996908, 10.88205029486207742 ) ) ;
#629=ORIENTED_EDGE ( 'NONE', *, *, #80597, .T. ) ;
#630=CARTESIAN_POINT ( 'NONE',  ( -103.5228709571500758, -23.48786465467241769, 11.44779295918254114 ) ) ;
#631=CARTESIAN_POINT ( 'NONE',  ( -50.18456845782914399, -25.03449303489322020, 7.555577232638461815 ) ) ;
#632=CARTESIAN_POINT ( 'NONE',  ( -68.63108587404039440, -24.35071581493542681, 9.817618358456032368 ) ) ;
#633=CARTESIAN_POINT ( 'NONE',  ( -15.36756058500021282, 13.76162614515376426, -1.500000000000002220 ) ) ;
#635=CARTESIAN_POINT ( 'NONE',  ( -2.642555958445479192, -21.45212208726272607, 11.49999999999999645 ) ) ;
#637=CARTESIAN_POINT ( 'NONE',  ( -46.62287095715004881, -24.64965695001467694, 8.947790433994185832 ) ) ;
#639=CARTESIAN_POINT ( 'NONE',  ( -6.430504157862594994, -21.42354456762059201, -1.500000000000002220 ) ) ;
#640=CARTESIAN_POINT ( 'NONE',  ( -47.54693701500606551, -24.15620529776627379, 10.23563542870660825 ) ) ;
#642=VERTEX_POINT ( 'NONE', #43407 ) ;
#643=CARTESIAN_POINT ( 'NONE',  ( -117.7763468626476850, -25.31365013357615368, 6.500921039148880531 ) ) ;
#644=CARTESIAN_POINT ( 'NONE',  ( -76.62287095715009855, -23.95044443724992433, 10.65354141964649948 ) ) ;
#646=CARTESIAN_POINT ( 'NONE',  ( -0.7727808018759799724, -20.89725122839497828, -1.500000000000002220 ) ) ;
#648=FACE_OUTER_BOUND ( 'NONE', #26996, .T. ) ;
#651=CARTESIAN_POINT ( 'NONE',  ( -128.6228709571500417, -23.47596703998600631, 11.44779298504227860 ) ) ;
#652=CARTESIAN_POINT ( 'NONE',  ( 15.88363568188429653, -14.04911357082368006, -1.500000000000002220 ) ) ;
#655=CARTESIAN_POINT ( 'NONE',  ( -69.62287095715005592, -23.48783264082478084, -1.443836473390067265 ) ) ;
#656=CARTESIAN_POINT ( 'NONE',  ( -20.50126671893153940, -7.481214725051755110, -1.500000000000002220 ) ) ;
#658=CARTESIAN_POINT ( 'NONE',  ( -76.52212335552069078, -23.48786465467240703, 11.44779295918254647 ) ) ;
#660=CARTESIAN_POINT ( 'NONE',  ( 12.66963027563507005, -17.75133666976559255, -1.500000000000002220 ) ) ;
#662=ORIENTED_EDGE ( 'NONE', *, *, #86913, .T. ) ;
#668=ORIENTED_EDGE ( 'NONE', *, *, #7979, .F. ) ;
#669=EDGE_CURVE ( 'NONE', #38959, #72936, #20443, .T. ) ;
#671=CARTESIAN_POINT ( 'NONE',  ( -28.72238104702265105, -24.94777617903022460, 2.725261753396577280 ) ) ;
#673=CARTESIAN_POINT ( 'NONE',  ( -6.347832186973104029, -20.24257907634199682, -1.500000000000002220 ) ) ;
#674=CARTESIAN_POINT ( 'NONE',  ( -94.51866586401287407, -23.73766607897670156, -1.055555164236450905 ) ) ;
#675=CARTESIAN_POINT ( 'NONE',  ( -79.88583274576632220, -25.27791948829852586, 7.452192272885968194 ) ) ;
#677=LINE ( 'NONE', #8797, #47034 ) ;
#679=CARTESIAN_POINT ( 'NONE',  ( 0.06232057257353295493, 19.38168652127415825, -1.500000000000002220 ) ) ;
#681=CARTESIAN_POINT ( 'NONE',  ( -70.23274567164976645, -25.31150975387220825, 5.317581533080277367 ) ) ;
#682=ORIENTED_EDGE ( 'NONE', *, *, #31445, .F. ) ;
#683=CARTESIAN_POINT ( 'NONE',  ( -3.338044803349280443, -19.22079736023769669, 11.49999999999999645 ) ) ;
#684=FACE_OUTER_BOUND ( 'NONE', #2410, .T. ) ;
#685=CARTESIAN_POINT ( 'NONE',  ( -107.5895376238167387, -24.65952944569304250, 1.056160979905697683 ) ) ;
#686=ORIENTED_EDGE ( 'NONE', *, *, #93583, .T. ) ;
#689=CARTESIAN_POINT ( 'NONE',  ( -70.74026866089612042, -25.30511070033976395, 4.894904393956083233 ) ) ;
#690=PLANE ( 'NONE',  #1809 ) ;
#692=CARTESIAN_POINT ( 'NONE',  ( 9.421224358276909072, -17.24829524558457194, -1.500000000000002220 ) ) ;
#693=B_SPLINE_CURVE_WITH_KNOTS ( 'NONE', 3,
 ( #53453, #45830, #13000, #66827, #15360, #59703 ),
 .UNSPECIFIED., .F., .F.,
 ( 4, 2, 4 ),
 ( 0.000000000000000000, 0.001380764517854760629, 0.002761529035709521258 ),
 .UNSPECIFIED. ) ;
#695=ORIENTED_EDGE ( 'NONE', *, *, #80167, .T. ) ;
#696=CARTESIAN_POINT ( 'NONE',  ( 0.9236959384754221958, 21.56878955078795812, -1.500000000000002220 ) ) ;
#697=CARTESIAN_POINT ( 'NONE',  ( -40.62644336949313129, -24.92564183028978775, 1.928384488918254203 ) ) ;
#698=DIRECTION ( 'NONE',  ( -1.000000000000000000, -3.773278334444166432E-23, -8.201307841325785021E-29 ) ) ;
#699=CARTESIAN_POINT ( 'NONE',  ( 23.03040035405544472, 1.057182387018521963, -1.500000000000002220 ) ) ;
#701=CARTESIAN_POINT ( 'NONE',  ( -74.58953762381673869, -23.47596703998600276, 11.44779298504227683 ) ) ;
#702=CARTESIAN_POINT ( 'NONE',  ( -130.5728709571500588, -23.56000036390797092, -1.497999999999531040 ) ) ;
#703=CARTESIAN_POINT ( 'NONE',  ( -121.5573564770503481, -23.48786465467241769, 11.44779295918253759 ) ) ;
#704=CARTESIAN_POINT ( 'NONE',  ( -100.5429575306527141, -25.04353918802791057, 7.561013281394894925 ) ) ;
#706=CARTESIAN_POINT ( 'NONE',  ( -129.5560488346142733, -23.73766607897671221, -1.055555164236443577 ) ) ;
#707=B_SPLINE_CURVE_WITH_KNOTS ( 'NONE', 3,
 ( #87065, #79953, #96189, #10439 ),
 .UNSPECIFIED., .F., .F.,
 ( 4, 4 ),
 ( 0.000000000000000000, 9.999999999998897304E-05 ),
 .UNSPECIFIED. ) ;
#708=CARTESIAN_POINT ( 'NONE',  ( -99.52609871227460303, -25.26400865036767485, 4.842596224614812428 ) ) ;
#709=CARTESIAN_POINT ( 'NONE',  ( -19.77041435686880533, -2.435487021107205940, -1.500000000000002220 ) ) ;
#711=CARTESIAN_POINT ( 'NONE',  ( -17.21045110277357182, -9.822940424218707278, -1.500000000000002220 ) ) ;
#713=CARTESIAN_POINT ( 'NONE',  ( -39.73251464975087544, -25.29116557167905555, 3.010156479320208689 ) ) ;
#716=CARTESIAN_POINT ( 'NONE',  ( -15.27568272636907665, 14.01247568063241999, 11.49999999999999645 ) ) ;
#717=CARTESIAN_POINT ( 'NONE',  ( -101.6228709571500701, -23.47596703998600631, 11.44779298504227683 ) ) ;
#718=CARTESIAN_POINT ( 'NONE',  ( -106.6228709571500559, -24.66019654487199730, 8.947790411086122830 ) ) ;
#719=CARTESIAN_POINT ( 'NONE',  ( 19.62911079104473444, -11.51699945595908758, 11.49999999999999645 ) ) ;
#722=CARTESIAN_POINT ( 'NONE',  ( -69.58785280780001870, -24.34968618360933945, 0.1864209137778826408 ) ) ;
#724=EDGE_CURVE ( 'NONE', #36801, #45447, #208, .T. ) ;
#726=CARTESIAN_POINT ( 'NONE',  ( 12.43249465596513126, -15.92577207200969092, -1.500000000000002220 ) ) ;
#727=LINE ( 'NONE', #23045, #75918 ) ;
#728=EDGE_CURVE ( 'NONE', #23841, #79650, #27659, .T. ) ;
#731=ORIENTED_EDGE ( 'NONE', *, *, #77412, .T. ) ;
#732=ADVANCED_FACE ( 'NONE', ( #15922 ), #55009, .F. ) ;
#733=VERTEX_POINT ( 'NONE', #24036 ) ;
#734=FACE_OUTER_BOUND ( 'NONE', #68634, .T. ) ;
#735=CARTESIAN_POINT ( 'NONE',  ( 16.68310095749102118, 15.68496000196893370, 11.49999999999998934 ) ) ;
#736=CARTESIAN_POINT ( 'NONE',  ( -50.90914965406638260, -25.27420588080167718, 3.408962287336470887 ) ) ;
#737=CARTESIAN_POINT ( 'NONE',  ( 18.46943957830784555, -11.30625484363265265, -1.500000000000002220 ) ) ;
#738=CARTESIAN_POINT ( 'NONE',  ( -36.62287095715006302, -23.72773821059535493, 11.05748984161097681 ) ) ;
#739=CARTESIAN_POINT ( 'NONE',  ( 16.07097863352054290, 13.35096362007907622, 11.49999999999999645 ) ) ;
#742=CARTESIAN_POINT ( 'NONE',  ( -73.52287095715007581, -23.48786465467241058, 11.44779295918254647 ) ) ;
#743=CARTESIAN_POINT ( 'NONE',  ( -124.6238252180020396, -24.51314013834316086, 0.6176544820404203939 ) ) ;
#744=CARTESIAN_POINT ( 'NONE',  ( -10.13730173486854369, -19.54584281717935568, 11.49999999999998934 ) ) ;
#745=VECTOR ( 'NONE', #16065, 1000.000000000000114 ) ;
#749=CARTESIAN_POINT ( 'NONE',  ( -49.59807878744301490, -25.18440185366671358, 3.677862597024960323 ) ) ;
#751=ORIENTED_EDGE ( 'NONE', *, *, #1684, .T. ) ;
#752=CARTESIAN_POINT ( 'NONE',  ( -123.6228709571500701, -23.72773821059535848, 11.05748984161097503 ) ) ;
#754=EDGE_LOOP ( 'NONE', ( #42777, #20631, #2418, #87464 ) ) ;
#755=CARTESIAN_POINT ( 'NONE',  ( -106.6228709571500985, -23.96127896941632329, -0.6493128931037804863 ) ) ;
#756=LINE ( 'NONE', #77367, #21131 ) ;
#758=CARTESIAN_POINT ( 'NONE',  ( 4.362881659454829197, 20.01674633476859810, -1.500000000000002220 ) ) ;
#762=CARTESIAN_POINT ( 'NONE',  ( -71.62287095715004170, -24.51387760970724372, 9.387446482453425389 ) ) ;
#765=CARTESIAN_POINT ( 'NONE',  ( 10.93216147639808611, 19.43004700418156361, 11.49999999999998934 ) ) ;
#767=CARTESIAN_POINT ( 'NONE',  ( -90.52287095715006160, -23.47593901973090524, -1.443836447538996426 ) ) ;
#772=DIRECTION ( 'NONE',  ( 0.000000000000000000, 0.9999999999976377785, 2.173523156925979975E-06 ) ) ;
#773=CARTESIAN_POINT ( 'NONE',  ( 15.94631523246878579, 13.42178585792578360, 11.49999999999998934 ) ) ;
#776=EDGE_CURVE ( 'NONE', #85237, #35109, #65247, .T. ) ;
#778=ORIENTED_EDGE ( 'NONE', *, *, #93642, .F. ) ;
#779=CARTESIAN_POINT ( 'NONE',  ( -58.52287095715006160, -23.47596703998600631, 11.44779298504228926 ) ) ;
#780=CARTESIAN_POINT ( 'NONE',  ( -13.85205798638896901, 15.75786377350088507, -1.500000000000002220 ) ) ;
#782=CARTESIAN_POINT ( 'NONE',  ( -69.52287095715007581, -23.73934037231756022, 11.05740245334329330 ) ) ;
#785=CARTESIAN_POINT ( 'NONE',  ( -106.5228709571500758, -29.50248528299804818, 1.056150453629043584 ) ) ;
#786=FACE_OUTER_BOUND ( 'NONE', #65075, .T. ) ;
#787=CARTESIAN_POINT ( 'NONE',  ( -118.5228709571500758, -23.47596703998600631, 11.44779298504227860 ) ) ;
#788=CARTESIAN_POINT ( 'NONE',  ( 12.10043277420606778, 18.60588626676543100, 11.49999999999999645 ) ) ;
#789=ORIENTED_EDGE ( 'NONE', *, *, #58186, .F. ) ;
#790=CARTESIAN_POINT ( 'NONE',  ( -44.52287095715006160, -29.50250786944525672, 11.44777988621624232 ) ) ;
#792=ORIENTED_EDGE ( 'NONE', *, *, #8058, .T. ) ;
#793=CARTESIAN_POINT ( 'NONE',  ( -22.46375958613465684, 3.124547546656453179, 11.49999999999998934 ) ) ;
#794=EDGE_CURVE ( 'NONE', #47537, #59400, #86947, .T. ) ;
#799=DIRECTION ( 'NONE',  ( 0.000000000000000000, -0.9999999999976377785, -2.173523156925979975E-06 ) ) ;
#801=CARTESIAN_POINT ( 'NONE',  ( 19.31759285448427477, -5.727529672960866236, -1.500000000000002220 ) ) ;
#802=CARTESIAN_POINT ( 'NONE',  ( -80.62287095715004170, -24.63287334234178871, 0.9662140553045442948 ) ) ;
#803=VERTEX_POINT ( 'NONE', #71229 ) ;
#805=CARTESIAN_POINT ( 'NONE',  ( -22.19192207843486386, -2.872123673023632584, -1.500000000000002220 ) ) ;
#806=B_SPLINE_CURVE_WITH_KNOTS ( 'NONE', 3,
 ( #95087, #80363, #46546, #70382 ),
 .UNSPECIFIED., .F., .F.,
 ( 4, 4 ),
 ( 0.000000000000000000, 9.999999999998900014E-05 ),
 .UNSPECIFIED. ) ;
#809=EDGE_LOOP ( 'NONE', ( #59193, #38629, #23114, #8310 ) ) ;
#811=CARTESIAN_POINT ( 'NONE',  ( -94.62789002903245716, -24.35071581493543036, 9.817618358456030592 ) ) ;
#814=CARTESIAN_POINT ( 'NONE',  ( -63.93038602344318377, -24.37807914296826084, 0.3010598746230576661 ) ) ;
#815=CARTESIAN_POINT ( 'NONE',  ( -5.392953615240748455, 18.82278424538476713, 11.49999999999998934 ) ) ;
#816=CARTESIAN_POINT ( 'NONE',  ( -102.5228709571500616, -24.51283580621452884, 0.6167428607045936095 ) ) ;
#818=CARTESIAN_POINT ( 'NONE',  ( 8.645823604709390153, 19.67543227842514852, 11.49999999999998934 ) ) ;
#821=CARTESIAN_POINT ( 'NONE',  ( -117.9228709571500673, -23.47593901973090524, -1.443836447538996426 ) ) ;
#823=CARTESIAN_POINT ( 'NONE',  ( 20.41593879258296695, -10.28030303932802880, -1.500000000000002220 ) ) ;
#827=CARTESIAN_POINT ( 'NONE',  ( -70.83259324169414128, -25.30884602800411542, 5.409333232728893215 ) ) ;
#828=CARTESIAN_POINT ( 'NONE',  ( 2.999408428739025023, -19.78128511538675127, 11.49999999999999645 ) ) ;
#829=FACE_OUTER_BOUND ( 'NONE', #39415, .T. ) ;
#830=CARTESIAN_POINT ( 'NONE',  ( -107.5228709571500758, -24.64898659630367916, 1.056161002820831474 ) ) ;
#833=VERTEX_POINT ( 'NONE', #64644 ) ;
#835=VECTOR ( 'NONE', #24110, 1000.000000000000114 ) ;
#836=CARTESIAN_POINT ( 'NONE',  ( -21.33044368757495590, -4.375833669458513597, -1.500000000000002220 ) ) ;
#837=CARTESIAN_POINT ( 'NONE',  ( -117.5895376238167245, -23.48783264082479505, -1.443836473390058384 ) ) ;
#838=CARTESIAN_POINT ( 'NONE',  ( 19.59260286812380514, -1.442238090573773501, -1.500000000000002220 ) ) ;
#839=VECTOR ( 'NONE', #13846, 1000.000000000000114 ) ;
#841=B_SPLINE_CURVE_WITH_KNOTS ( 'NONE', 3,
 ( #34192, #48421, #56038, #33689 ),
 .UNSPECIFIED., .F., .F.,
 ( 4, 4 ),
 ( 0.4007861916091369769, 0.4097926228812525662 ),
 .UNSPECIFIED. ) ;
#842=CARTESIAN_POINT ( 'NONE',  ( -104.6228709571500559, -23.48786465467241413, 11.44779295918254114 ) ) ;
#844=CARTESIAN_POINT ( 'NONE',  ( -91.58604265345489637, -24.51419770103159124, 9.386484678747176957 ) ) ;
#846=CARTESIAN_POINT ( 'NONE',  ( -0.1859688948871585645, 20.53422428922035081, 11.49999999999999645 ) ) ;
#847=DIRECTION ( 'NONE',  ( 0.000000000000000000, 2.173523156925980399E-06, -0.9999999999976378895 ) ) ;
#848=CARTESIAN_POINT ( 'NONE',  ( -120.5186651893930332, -24.40034930558991633, 0.3402023900116107336 ) ) ;
#849=CARTESIAN_POINT ( 'NONE',  ( 3.115699594417459473, -22.39947108414558485, 11.49999999999999645 ) ) ;
#852=ADVANCED_FACE ( 'NONE', ( #2225 ), #99180, .T. ) ;
#853=CARTESIAN_POINT ( 'NONE',  ( -99.53249707683190195, -25.26387314544760798, 4.095394624650092297 ) ) ;
#854=CARTESIAN_POINT ( 'NONE',  ( -37.52287095715009713, -24.33832256527048798, 0.1851278514138569864 ) ) ;
#855=CARTESIAN_POINT ( 'NONE',  ( -125.6246426838371661, -24.40133493613050675, 9.663955038902798833 ) ) ;
#857=CARTESIAN_POINT ( 'NONE',  ( -85.62287095715004170, -24.83602698348159166, 1.605859176311267955 ) ) ;
#858=EDGE_CURVE ( 'NONE', #31747, #84710, #60382, .T. ) ;
#859=CARTESIAN_POINT ( 'NONE',  ( -33.62287095715004881, -24.50216790748205042, 0.6166512839542545033 ) ) ;
#860=ADVANCED_FACE ( 'NONE', ( #87444 ), #66138, .T. ) ;
#864=CARTESIAN_POINT ( 'NONE',  ( -20.32320236877023589, 10.94715076914730290, 11.49999999999999645 ) ) ;
#865=CARTESIAN_POINT ( 'NONE',  ( 22.20583189720066741, -5.198064566299082756, 11.49999999999998934 ) ) ;
#866=CARTESIAN_POINT ( 'NONE',  ( -74.59223927811392230, -24.15543982623907127, -0.2315651400026650930 ) ) ;
#867=CARTESIAN_POINT ( 'NONE',  ( -115.5228709571500758, -23.84081130425358097, 10.88220057483157888 ) ) ;
#868=CARTESIAN_POINT ( 'NONE',  ( -57.52287095715007581, -23.72747288104470087, -1.053458166803227014 ) ) ;
#869=AXIS2_PLACEMENT_3D ( 'NONE', #18946, #2744, #41811 ) ;
#870=CARTESIAN_POINT ( 'NONE',  ( 21.67916507323446496, -5.852930566066080864, 11.49999999999999645 ) ) ;
#872=CARTESIAN_POINT ( 'NONE',  ( -84.52287095715006160, -23.72747288104470087, -1.053458166803226126 ) ) ;
#873=CARTESIAN_POINT ( 'NONE',  ( -43.52287095715008292, -24.33927499327853639, 9.819080762295813614 ) ) ;
#874=CARTESIAN_POINT ( 'NONE',  ( 21.59112034314636119, 3.954845139028329015, 11.49999999999998934 ) ) ;
#876=CARTESIAN_POINT ( 'NONE',  ( -44.48278020699296320, -24.66019654487199020, 8.947790411086115725 ) ) ;
#877=DIRECTION ( 'NONE',  ( -3.773278334444167608E-23, 1.000000000000000000, 0.000000000000000000 ) ) ;
#878=EDGE_LOOP ( 'NONE', ( #26481, #100063 ) ) ;
#879=CARTESIAN_POINT ( 'NONE',  ( -112.5228709571500616, -23.48786465467241769, 11.44779295918253936 ) ) ;
#880=CARTESIAN_POINT ( 'NONE',  ( -66.62287095715005592, -29.50247984919015209, -1.443849546365055359 ) ) ;
#882=CARTESIAN_POINT ( 'NONE',  ( -12.74120943341865342, -16.01528480738631899, -1.500000000000002220 ) ) ;
#884=VERTEX_POINT ( 'NONE', #79824 ) ;
#886=ORIENTED_EDGE ( 'NONE', *, *, #84728, .F. ) ;
#887=CARTESIAN_POINT ( 'NONE',  ( -3.381418692465893105, -22.81955385325859709, -1.500000000000002220 ) ) ;
#888=CARTESIAN_POINT ( 'NONE',  ( -112.5228709571500758, -24.35013146730204170, 9.818937971375092388 ) ) ;
#889=CARTESIAN_POINT ( 'NONE',  ( 2.300710779914242110, 20.15441874099239783, -1.500000000000002220 ) ) ;
#890=ORIENTED_EDGE ( 'NONE', *, *, #15558, .F. ) ;
#892=CARTESIAN_POINT ( 'NONE',  ( -92.54440427696837901, -24.65952944569304961, 1.056160979905703901 ) ) ;
#893=CARTESIAN_POINT ( 'NONE',  ( -40.22287095715006444, -23.47596703998600276, 11.44779298504227683 ) ) ;
#895=CARTESIAN_POINT ( 'NONE',  ( 21.44729954461699251, -1.519088741117538000, 11.49999999999999645 ) ) ;
#896=VERTEX_POINT ( 'NONE', #88950 ) ;
#897=CARTESIAN_POINT ( 'NONE',  ( -75.53432955309628483, -25.00158670708910691, 2.256160236439223699 ) ) ;
#898=CARTESIAN_POINT ( 'NONE',  ( -61.50934325614997533, -23.96169478059712787, 10.65365249895718591 ) ) ;
#900=CARTESIAN_POINT ( 'NONE',  ( 14.61947915221463923, 14.71393552341326760, 11.49999999999998934 ) ) ;
#903=CARTESIAN_POINT ( 'NONE',  ( -91.58953762381672448, -24.64898659630368627, 1.056161002820390937 ) ) ;
#906=CARTESIAN_POINT ( 'NONE',  ( -111.6258004380657667, -24.35071581493544457, 9.817618358456018157 ) ) ;
#908=VERTEX_POINT ( 'NONE', #11817 ) ;
#909=VERTEX_POINT ( 'NONE', #3236 ) ;
#911=CARTESIAN_POINT ( 'NONE',  ( -42.58700419767085776, -24.35071581493543036, 9.817618358456037697 ) ) ;
#914=CARTESIAN_POINT ( 'NONE',  ( -20.57682416348112397, 7.868404785394932155, 11.49999999999999645 ) ) ;
#916=CARTESIAN_POINT ( 'NONE',  ( -89.51147662468558508, -24.15620529776628445, 10.23563542870660115 ) ) ;
#917=CARTESIAN_POINT ( 'NONE',  ( -22.55165446212525993, 1.111233042438415808, 11.49999999999998934 ) ) ;
#918=AXIS2_PLACEMENT_3D ( 'NONE', #95863, #26357, #9125 ) ;
#919=CARTESIAN_POINT ( 'NONE',  ( 16.07406896385161943, -13.52096256729613266, -1.500000000000002220 ) ) ;
#922=VERTEX_POINT ( 'NONE', #41276 ) ;
#923=VERTEX_POINT ( 'NONE', #72230 ) ;
#924=CARTESIAN_POINT ( 'NONE',  ( -59.62287095715004170, -23.72773821059535848, 11.05748984161097503 ) ) ;
#925=EDGE_CURVE ( 'NONE', #37824, #10565, #2724, .T. ) ;
#927=CARTESIAN_POINT ( 'NONE',  ( -113.6228709571500559, -24.64965695001469115, 8.947790433994176951 ) ) ;
#929=CARTESIAN_POINT ( 'NONE',  ( 18.68757921870947669, -9.911485057863893999, -1.500000000000002220 ) ) ;
#931=CARTESIAN_POINT ( 'NONE',  ( -51.93149462243456327, -25.03148440107001349, 6.174051623307587278 ) ) ;
#932=PLANE ( 'NONE',  #63196 ) ;
#933=LINE ( 'NONE', #45613, #45946 ) ;
#935=CARTESIAN_POINT ( 'NONE',  ( -19.06252244145942498, 11.34236556261432405, -1.500000000000002220 ) ) ;
#937=VERTEX_POINT ( 'NONE', #35666 ) ;
#938=CARTESIAN_POINT ( 'NONE',  ( -51.44679290749079570, -25.24860047834440380, 5.195306865420171505 ) ) ;
#939=CARTESIAN_POINT ( 'NONE',  ( -37.50486701413690582, -23.96119346886880663, -0.6495511937831990323 ) ) ;
#940=CARTESIAN_POINT ( 'NONE',  ( -40.41248649115142655, -25.30361164129646667, 5.542177216901341907 ) ) ;
#941=CARTESIAN_POINT ( 'NONE',  ( -37.52287095715006870, -29.50250243563736774, 8.947779886222148704 ) ) ;
#942=CARTESIAN_POINT ( 'NONE',  ( -33.62287095715005592, -24.64965695001467694, 8.947790433994189385 ) ) ;
#943=CARTESIAN_POINT ( 'NONE',  ( -3.206006181753352724, -19.19236486397402430, 11.49999999999998934 ) ) ;
#945=CARTESIAN_POINT ( 'NONE',  ( 19.99361899508246765, -7.638522130635823082, 11.49999999999998934 ) ) ;
#947=CARTESIAN_POINT ( 'NONE',  ( -60.53567020741864013, -24.73531770709804078, 8.716586749031112191 ) ) ;
#948=B_SPLINE_CURVE_WITH_KNOTS ( 'NONE', 3,
 ( #77472, #76473, #31821, #61779 ),
 .UNSPECIFIED., .F., .F.,
 ( 4, 4 ),
 ( 0.000000000000000000, 0.0001000000000000167422 ),
 .UNSPECIFIED. ) ;
#950=DIRECTION ( 'NONE',  ( -3.773278334453079618E-23, 0.9999999999976377785, 2.173523156925979975E-06 ) ) ;
#951=CARTESIAN_POINT ( 'NONE',  ( 7.379361219544559702, 21.46082085352547963, -1.500000000000002220 ) ) ;
#953=CARTESIAN_POINT ( 'NONE',  ( -101.7776484685884242, -29.50249165161862663, 3.986241424695394109 ) ) ;
#954=CARTESIAN_POINT ( 'NONE',  ( -11.18921147948170614, -16.41150865552512883, 11.49999999999999645 ) ) ;
#956=CARTESIAN_POINT ( 'NONE',  ( -115.5562042904833930, -23.47596703998600631, 11.44779298504227683 ) ) ;
#958=ORIENTED_EDGE ( 'NONE', *, *, #76806, .T. ) ;
#961=FACE_OUTER_BOUND ( 'NONE', #23845, .T. ) ;
#962=CARTESIAN_POINT ( 'NONE',  ( -10.61912389536305490, -18.88692380039396213, -1.500000000000002220 ) ) ;
#963=CARTESIAN_POINT ( 'NONE',  ( -32.52287095715003318, -24.66019654487198665, 8.947790411086131712 ) ) ;
#964=CARTESIAN_POINT ( 'NONE',  ( 19.19537281719634336, 3.394423509666608663, -1.500000000000002220 ) ) ;
#965=CARTESIAN_POINT ( 'NONE',  ( -55.62373614600970484, -25.00182538069146432, 7.747789668545041586 ) ) ;
#966=ADVANCED_FACE ( 'NONE', ( #4713 ), #44278, .F. ) ;
#967=B_SPLINE_CURVE_WITH_KNOTS ( 'NONE', 3,
 ( #57525, #87455, #75217, #13308, #59017, #73728 ),
 .UNSPECIFIED., .F., .F.,
 ( 4, 2, 4 ),
 ( 0.000000000000000000, 0.001381509804613668827, 0.002763019609227337654 ),
 .UNSPECIFIED. ) ;
#969=CARTESIAN_POINT ( 'NONE',  ( -17.41452279269062586, 10.58001483151439004, 11.49999999999999645 ) ) ;
#970=CARTESIAN_POINT ( 'NONE',  ( -75.62287095715005592, -29.50248528299804818, 1.056150453629038477 ) ) ;
#972=CARTESIAN_POINT ( 'NONE',  ( -112.5228709571500616, -29.50248528299804818, 1.056150453629043584 ) ) ;
#973=ORIENTED_EDGE ( 'NONE', *, *, #55206, .F. ) ;
#974=CARTESIAN_POINT ( 'NONE',  ( -30.62155233649868791, -24.14929313691196455, 10.49653219292474482 ) ) ;
#975=DIRECTION ( 'NONE',  ( 0.000000000000000000, 2.173523156925980399E-06, -0.9999999999976378895 ) ) ;
#976=CARTESIAN_POINT ( 'NONE',  ( -48.92504535501358021, -25.25214610244555402, 5.781339582145927025 ) ) ;
#978=EDGE_CURVE ( 'NONE', #73446, #63682, #95404, .T. ) ;
#979=CARTESIAN_POINT ( 'NONE',  ( -40.46892088308801050, -25.00182538069146432, 7.747789668545040698 ) ) ;
#981=CARTESIAN_POINT ( 'NONE',  ( 15.17442925503088169, 13.16703847180013831, -1.500000000000002220 ) ) ;
#982=CARTESIAN_POINT ( 'NONE',  ( -109.5222136733952425, -23.48783264082476663, -1.443836473390089692 ) ) ;
#983=EDGE_CURVE ( 'NONE', #84470, #85538, #62713, .T. ) ;
#988=B_SPLINE_CURVE_WITH_KNOTS ( 'NONE', 3,
 ( #63516, #24426, #84820, #46266, #93, #55901 ),
 .UNSPECIFIED., .F., .F.,
 ( 4, 2, 4 ),
 ( 6.384118678609355280E-06, 0.001386860460828372816, 0.002767336802978136254 ),
 .UNSPECIFIED. ) ;
#989=CARTESIAN_POINT ( 'NONE',  ( -16.74478417649319084, -15.65585335247391896, 11.49999999999999645 ) ) ;
#990=CARTESIAN_POINT ( 'NONE',  ( -22.17926634000774655, 4.976981427743210951, -1.500000000000002220 ) ) ;
#991=VERTEX_POINT ( 'NONE', #66636 ) ;
#992=CARTESIAN_POINT ( 'NONE',  ( -53.62287095715004881, -23.48786465467241058, 11.44779295918255002 ) ) ;
#994=FACE_OUTER_BOUND ( 'NONE', #44526, .T. ) ;
#995=CARTESIAN_POINT ( 'NONE',  ( -38.60080858671575044, -23.96169478059712432, 10.65365249895718591 ) ) ;
#996=EDGE_CURVE ( 'NONE', #93569, #23708, #38610, .T. ) ;
#997=CARTESIAN_POINT ( 'NONE',  ( -30.57287095715006231, -24.76473628883709210, 8.626942252220645813 ) ) ;
#999=LINE ( 'NONE', #16714, #29049 ) ;
#1001=CARTESIAN_POINT ( 'NONE',  ( 4.102729645046709450, 19.96921287702725323, -1.500000000000002220 ) ) ;
#1002=EDGE_LOOP ( 'NONE', ( #73125, #62557, #56487, #47720 ) ) ;
#1003=B_SPLINE_CURVE_WITH_KNOTS ( 'NONE', 3,
 ( #3545, #34489, #96382, #65465 ),
 .UNSPECIFIED., .F., .F.,
 ( 4, 4 ),
 ( 0.3990514020202980405, 0.4000521490610636222 ),
 .UNSPECIFIED. ) ;
#1004=ADVANCED_FACE ( 'NONE', ( #59498 ), #12802, .F. ) ;
#1005=CARTESIAN_POINT ( 'NONE',  ( -22.94451526424785115, -1.264959178018935315, 11.49999999999998934 ) ) ;
#1007=CARTESIAN_POINT ( 'NONE',  ( -54.54770071756311722, -24.15620529776628089, 10.23563542870661180 ) ) ;
#1009=AXIS2_PLACEMENT_3D ( 'NONE', #6067, #84185, #60383 ) ;
#1010=CARTESIAN_POINT ( 'NONE',  ( -114.5228709571500332, -23.73934037231757443, 11.05740245334327909 ) ) ;
#1011=CARTESIAN_POINT ( 'NONE',  ( -53.63292963077573461, -24.35071581493542681, 9.817618358456032368 ) ) ;
#1012=CARTESIAN_POINT ( 'NONE',  ( 14.64190796094839264, -15.47823801613018269, 11.49999999999999645 ) ) ;
#1014=EDGE_LOOP ( 'NONE', ( #26843, #62311, #71409, #34493 ) ) ;
#1015=CARTESIAN_POINT ( 'NONE',  ( -21.61287440533560300, 5.199345243644041936, 11.49999999999998934 ) ) ;
#1016=CARTESIAN_POINT ( 'NONE',  ( 19.39950376024442846, -7.079068461131618584, -1.500000000000002220 ) ) ;
#1018=CARTESIAN_POINT ( 'NONE',  ( -112.6228709571500275, -23.72773821059535493, 11.05748984161097503 ) ) ;
#1019=CARTESIAN_POINT ( 'NONE',  ( -95.59439228026970170, -24.15602025860896163, 10.28564288303536856 ) ) ;
#1021=CARTESIAN_POINT ( 'NONE',  ( -65.55620429048339304, -25.00158670708909625, 2.256160236439165967 ) ) ;
#1022=ORIENTED_EDGE ( 'NONE', *, *, #35675, .F. ) ;
#1025=CARTESIAN_POINT ( 'NONE',  ( -0.8937202392249329330, 20.86669477224961256, -1.500000000000002220 ) ) ;
#1026=CARTESIAN_POINT ( 'NONE',  ( -20.50126671893153940, -7.481214725051755110, 11.49999999999999645 ) ) ;
#1030=CARTESIAN_POINT ( 'NONE',  ( 3.503984654965784706, -22.18958196551723816, -1.500000000000002220 ) ) ;
#1032=CARTESIAN_POINT ( 'NONE',  ( -118.5523285634779285, -24.66019654487199730, 8.947790411086115725 ) ) ;
#1033=EDGE_CURVE ( 'NONE', #57047, #32034, #87223, .T. ) ;
#1036=EDGE_LOOP ( 'NONE', ( #90357, #82914, #11882, #85657 ) ) ;
#1037=B_SPLINE_CURVE_WITH_KNOTS ( 'NONE', 3,
 ( #83711, #77090, #7589, #22297, #6590, #13190, #44164, #53277 ),
 .UNSPECIFIED., .F., .F.,
 ( 4, 2, 2, 4 ),
 ( -0.001240666984356056379, -0.0002401179793396601269, 0.0007604310256767361255, 0.002761529035709532100 ),
 .UNSPECIFIED. ) ;
#1038=ORIENTED_EDGE ( 'NONE', *, *, #61912, .F. ) ;
#1039=ORIENTED_EDGE ( 'NONE', *, *, #99470, .T. ) ;
#1042=EDGE_LOOP ( 'NONE', ( #24675, #4803, #49008, #11806 ) ) ;
#1043=VECTOR ( 'NONE', #77178, 1000.000000000000114 ) ;
#1044=CARTESIAN_POINT ( 'NONE',  ( 9.194277187580093269, -19.27880637823015419, -1.500000000000002220 ) ) ;
#1045=CARTESIAN_POINT ( 'NONE',  ( -22.19192207843486386, -2.872123673023632584, 11.49999999999999645 ) ) ;
#1047=EDGE_LOOP ( 'NONE', ( #92275, #38229, #66850, #54927 ) ) ;
#1048=VECTOR ( 'NONE', #3635, 1000.000000000000114 ) ;
#1049=CARTESIAN_POINT ( 'NONE',  ( -1.165634184549018126, -21.02984315360824752, 11.49999999999998934 ) ) ;
#1050=CARTESIAN_POINT ( 'NONE',  ( -30.60107339264236259, -24.67525583858868643, 1.095666116063849449 ) ) ;
#1051=CARTESIAN_POINT ( 'NONE',  ( 13.74685606122050885, 14.44317598224977672, -1.500000000000002220 ) ) ;
#1055=CARTESIAN_POINT ( 'NONE',  ( -21.79611004543898289, 2.820803583321412678, -1.500000000000002220 ) ) ;
#1056=CARTESIAN_POINT ( 'NONE',  ( -87.52287095714999055, -23.94994826722564696, -0.6494450866342719175 ) ) ;
#1059=DIRECTION ( 'NONE',  ( -3.773278334453079030E-23, 0.9999999999976377785, 2.173523156925979128E-06 ) ) ;
#1060=CARTESIAN_POINT ( 'NONE',  ( 18.01467621842780176, -10.50282939286117667, 11.49999999999999645 ) ) ;
#1064=CARTESIAN_POINT ( 'NONE',  ( -117.5228709571500616, -23.73907113216989728, -1.053371485793242357 ) ) ;
#1065=CARTESIAN_POINT ( 'NONE',  ( 3.515848477382193416, 21.04717058667041130, 11.49999999999998934 ) ) ;
#1066=DIRECTION ( 'NONE',  ( -1.000000000000000000, -3.773278334444167608E-23, -8.201307833595939069E-29 ) ) ;
#1067=CARTESIAN_POINT ( 'NONE',  ( -117.5228709571500758, -24.51387760970726504, 9.387446482453405849 ) ) ;
#1071=CARTESIAN_POINT ( 'NONE',  ( -1.585881643086899606, 22.48459252949185228, -1.500000000000002220 ) ) ;
#1072=FACE_OUTER_BOUND ( 'NONE', #12168, .T. ) ;
#1073=EDGE_LOOP ( 'NONE', ( #75781, #8008, #64546, #16292 ) ) ;
#1074=CARTESIAN_POINT ( 'NONE',  ( -51.52532898735692868, -25.26458355271423528, 6.117596087636846036 ) ) ;
#1075=CARTESIAN_POINT ( 'NONE',  ( -31.49622502664552215, -24.15620529776627379, 10.23563542870661536 ) ) ;
#1076=CARTESIAN_POINT ( 'NONE',  ( -16.08770303010339831, 11.32657509950784736, 11.49999999999999645 ) ) ;
#1077=CARTESIAN_POINT ( 'NONE',  ( -28.62287095715006657, -24.50666107542846461, 1.056161637124864550 ) ) ;
#1079=ORIENTED_EDGE ( 'NONE', *, *, #35575, .T. ) ;
#1080=CARTESIAN_POINT ( 'NONE',  ( -99.51411512703360529, -24.15543982623907837, -0.2315651400026449425 ) ) ;
#1081=CARTESIAN_POINT ( 'NONE',  ( -59.52287095715006160, -24.64965694238407323, 8.947790433994201820 ) ) ;
#1083=B_SPLINE_CURVE_WITH_KNOTS ( 'NONE', 3,
 ( #84838, #100040, #85334, #8226, #70121, #30551, #38664, #92444 ),
 .UNSPECIFIED., .F., .F.,
 ( 4, 2, 2, 4 ),
 ( -0.001240355328177004729, -0.0002398155169400588947, 0.0007607242942968869392, 0.002761803916770778390 ),
 .UNSPECIFIED. ) ;
#1086=CARTESIAN_POINT ( 'NONE',  ( 0.5484783294719396407, -19.75002165935583776, 11.49999999999998934 ) ) ;
#1087=ORIENTED_EDGE ( 'NONE', *, *, #72726, .T. ) ;
#1088=VECTOR ( 'NONE', #73324, 1000.000000000000114 ) ;
#1089=CARTESIAN_POINT ( 'NONE',  ( -120.5228709571500048, -23.85229601348996198, 10.88205029486208097 ) ) ;
#1093=CARTESIAN_POINT ( 'NONE',  ( -107.6228709571500701, -24.65952944569304961, 1.056160979905703901 ) ) ;
#1094=CARTESIAN_POINT ( 'NONE',  ( -100.4304529591284307, -25.30235285477424867, 4.722036383736525345 ) ) ;
#1095=FACE_OUTER_BOUND ( 'NONE', #14726, .T. ) ;
#1097=CARTESIAN_POINT ( 'NONE',  ( -41.52287095715005449, -24.66019654487198665, 8.947790411086121054 ) ) ;
#1099=CARTESIAN_POINT ( 'NONE',  ( 2.999408428739025023, -19.78128511538675127, -1.500000000000002220 ) ) ;
#1101=CARTESIAN_POINT ( 'NONE',  ( -36.62287095715005592, -29.50247984919015209, -1.443849546365060466 ) ) ;
#1102=CARTESIAN_POINT ( 'NONE',  ( -116.5175123996784095, -24.35071581493543746, 9.817618358456021710 ) ) ;
#1103=ORIENTED_EDGE ( 'NONE', *, *, #49017, .T. ) ;
#1105=DIRECTION ( 'NONE',  ( -0.000000000000000000, 2.173523156925979552E-06, -0.9999999999976378895 ) ) ;
#1106=CARTESIAN_POINT ( 'NONE',  ( -110.3346797185884327, -25.18430153814381356, 3.293943118072274689 ) ) ;
#1108=LINE ( 'NONE', #45778, #75272 ) ;
#1109=CARTESIAN_POINT ( 'NONE',  ( -108.5228709571500474, -24.50216790748205042, 0.6166512839542558355 ) ) ;
#1110=EDGE_CURVE ( 'NONE', #52812, #39486, #60646, .T. ) ;
#1111=DIRECTION ( 'NONE',  ( -1.000000000000000000, -3.773278334444167608E-23, -8.201307833595939069E-29 ) ) ;
#1112=CARTESIAN_POINT ( 'NONE',  ( -83.64043043277688128, -23.73766607897670511, -1.055555164236457122 ) ) ;
#1114=CARTESIAN_POINT ( 'NONE',  ( -63.62287095715004881, -24.66019654487199020, 8.947790411086131712 ) ) ;
#1115=DIRECTION ( 'NONE',  ( -3.773278334453079030E-23, 0.9999999999976377785, 2.173523156925979128E-06 ) ) ;
#1119=CARTESIAN_POINT ( 'NONE',  ( 20.23811035156253979, -1.552196809741442696, -1.500000000000002220 ) ) ;
#1120=ADVANCED_FACE ( 'NONE', ( #78198 ), #85315, .T. ) ;
#1122=VECTOR ( 'NONE', #15146, 1000.000000000000114 ) ;
#1124=ORIENTED_EDGE ( 'NONE', *, *, #36022, .T. ) ;
#1125=CARTESIAN_POINT ( 'NONE',  ( -122.5228709571500616, -23.47596703998600631, 11.44779298504227860 ) ) ;
#1126=CARTESIAN_POINT ( 'NONE',  ( 11.25103634530202790, -16.72154935384561725, -1.500000000000002220 ) ) ;
#1127=CARTESIAN_POINT ( 'NONE',  ( 19.19679251752027227, 8.867671107084703408, 11.49999999999999645 ) ) ;
#1128=CARTESIAN_POINT ( 'NONE',  ( 20.57361055066190758, -8.084994430987380909, -1.500000000000002220 ) ) ;
#1129=B_SPLINE_CURVE_WITH_KNOTS ( 'NONE', 3,
 ( #52521, #22538, #53530, #29675 ),
 .UNSPECIFIED., .F., .F.,
 ( 4, 4 ),
 ( 0.000000000000000000, 9.999999999998897304E-05 ),
 .UNSPECIFIED. ) ;
#1130=CARTESIAN_POINT ( 'NONE',  ( -17.31529204923715071, 11.11782870402162260, 11.49999999999998934 ) ) ;
#1132=EDGE_LOOP ( 'NONE', ( #9244, #75305, #95750, #21316 ) ) ;
#1135=CARTESIAN_POINT ( 'NONE',  ( -70.27422298781921484, -25.31465149953924865, 4.851635142449610250 ) ) ;
#1136=PLANE ( 'NONE',  #35654 ) ;
#1140=CARTESIAN_POINT ( 'NONE',  ( -112.6228709571500701, -23.48783264082479150, -1.443836473390060160 ) ) ;
#1141=CARTESIAN_POINT ( 'NONE',  ( -55.55620429048339304, -24.99156044556202261, 7.747789690856174971 ) ) ;
#1143=CARTESIAN_POINT ( 'NONE',  ( -20.61657899823519813, -2.091364977790679980, -1.500000000000002220 ) ) ;
#1144=EDGE_CURVE ( 'NONE', #79651, #57540, #99254, .T. ) ;
#1145=CARTESIAN_POINT ( 'NONE',  ( -17.90551237062050305, -12.20792721910736667, 11.49999999999999645 ) ) ;
#1147=CARTESIAN_POINT ( 'NONE',  ( -42.52287095715005449, -23.47596703998600631, 11.44779298504229281 ) ) ;
#1148=VECTOR ( 'NONE', #51324, 1000.000000000000114 ) ;
#1150=CARTESIAN_POINT ( 'NONE',  ( -17.59303920844588376, -13.82112144285918731, 11.49999999999998934 ) ) ;
#1151=CARTESIAN_POINT ( 'NONE',  ( -47.49414261739990195, -24.35071581493542325, 9.817618358456030592 ) ) ;
#1152=CARTESIAN_POINT ( 'NONE',  ( -74.62287095715005592, -23.47596703998600631, 11.44779298504227860 ) ) ;
#1153=ADVANCED_FACE ( 'NONE', ( #47777 ), #93426, .T. ) ;
#1154=ORIENTED_EDGE ( 'NONE', *, *, #72807, .T. ) ;
#1155=CARTESIAN_POINT ( 'NONE',  ( -119.4728709572981984, -25.40561137786259138, 5.197919763437823804 ) ) ;
#1156=CARTESIAN_POINT ( 'NONE',  ( -35.58880974400002373, -24.52399227489126687, 9.353111116836519301 ) ) ;
#1163=CARTESIAN_POINT ( 'NONE',  ( -57.62287095715004881, -23.47596703998600276, 11.44779298504227683 ) ) ;
#1164=CARTESIAN_POINT ( 'NONE',  ( -9.521469661382619520, 18.92286876745961166, -1.500000000000002220 ) ) ;
#1166=CARTESIAN_POINT ( 'NONE',  ( -117.5162854265894623, -24.65952944569305316, 1.056160979905706343 ) ) ;
#1167=CARTESIAN_POINT ( 'NONE',  ( -21.44618410820073606, 4.064364382921047181, 11.49999999999998934 ) ) ;
#1168=FACE_OUTER_BOUND ( 'NONE', #5300, .T. ) ;
#1169=DIRECTION ( 'NONE',  ( 0.000000000000000000, 0.9999999999976377785, 2.173523156925979975E-06 ) ) ;
#1171=CARTESIAN_POINT ( 'NONE',  ( -21.80608713477256089, -0.9339522974687717305, -1.500000000000002220 ) ) ;
#1172=CARTESIAN_POINT ( 'NONE',  ( -95.52287095715011844, -23.48783264082477373, -1.443836473390086139 ) ) ;
#1173=ORIENTED_EDGE ( 'NONE', *, *, #95629, .F. ) ;
#1174=CARTESIAN_POINT ( 'NONE',  ( -41.62287095715006302, -23.94994826722565762, -0.6494450866342744710 ) ) ;
#1176=VERTEX_POINT ( 'NONE', #38141 ) ;
#1177=CARTESIAN_POINT ( 'NONE',  ( -51.62287095715005592, -23.48786465467241413, 11.44779295918254824 ) ) ;
#1179=ORIENTED_EDGE ( 'NONE', *, *, #4696, .T. ) ;
#1180=ORIENTED_EDGE ( 'NONE', *, *, #59638, .F. ) ;
#1181=PLANE ( 'NONE',  #19985 ) ;
#1182=CARTESIAN_POINT ( 'NONE',  ( -119.9228709571500531, -23.47593901973090524, -1.443836447538996426 ) ) ;
#1183=CARTESIAN_POINT ( 'NONE',  ( -18.66175431467001999, 10.11895122522205526, 11.49999999999998934 ) ) ;
#1184=FACE_OUTER_BOUND ( 'NONE', #87782, .T. ) ;
#1185=CARTESIAN_POINT ( 'NONE',  ( -130.5728709571501156, -25.56688301298834531, 3.825958421598583570 ) ) ;
#1186=DIRECTION ( 'NONE',  ( 0.000000000000000000, 0.9999999999976377785, 2.173523156925979128E-06 ) ) ;
#1188=DIRECTION ( 'NONE',  ( -3.773278334453079030E-23, 0.9999999999976377785, 2.173523156925979128E-06 ) ) ;
#1190=CARTESIAN_POINT ( 'NONE',  ( -0.1161231997828221785, -19.40653004597026410, -1.500000000000002220 ) ) ;
#1191=B_SPLINE_CURVE_WITH_KNOTS ( 'NONE', 3,
 ( #16673, #17174, #1969, #47141 ),
 .UNSPECIFIED., .F., .F.,
 ( 4, 4 ),
 ( 0.000000000000000000, 9.999999999997510880E-05 ),
 .UNSPECIFIED. ) ;
#1192=CARTESIAN_POINT ( 'NONE',  ( -39.03507040974603370, -25.03707806782366418, 7.590868867492675420 ) ) ;
#1194=CARTESIAN_POINT ( 'NONE',  ( 6.171429453590791425, 18.48145409631445446, 11.49999999999999645 ) ) ;
#1195=CARTESIAN_POINT ( 'NONE',  ( -42.52287095715005449, -23.72773821059535848, 11.05748984161097503 ) ) ;
#1196=EDGE_CURVE ( 'NONE', #1265, #86370, #80724, .T. ) ;
#1197=VECTOR ( 'NONE', #14138, 1000.000000000000114 ) ;
#1198=B_SPLINE_CURVE_WITH_KNOTS ( 'NONE', 3,
 ( #25871, #97383, #34985, #27867 ),
 .UNSPECIFIED., .F., .F.,
 ( 4, 4 ),
 ( 2.775557561562891043E-17, 9.999999999998898659E-05 ),
 .UNSPECIFIED. ) ;
#1199=CARTESIAN_POINT ( 'NONE',  ( -68.52287095715010423, -23.94994826722564696, -0.6494450866342724726 ) ) ;
#1202=EDGE_CURVE ( 'NONE', #34031, #27877, #13339, .T. ) ;
#1203=DIRECTION ( 'NONE',  ( -3.773278334444167608E-23, 1.000000000000000000, 0.000000000000000000 ) ) ;
#1205=CARTESIAN_POINT ( 'NONE',  ( -50.38822539166533687, -25.30267106383720943, 4.736250553104468075 ) ) ;
#1206=CARTESIAN_POINT ( 'NONE',  ( -93.52216986576536328, -23.48786465467241058, 11.44779295918254469 ) ) ;
#1207=CARTESIAN_POINT ( 'NONE',  ( -8.025172913017740939, -17.94849717234452768, 11.49999999999998934 ) ) ;
#1208=VERTEX_POINT ( 'NONE', #17822 ) ;
#1209=CARTESIAN_POINT ( 'NONE',  ( 21.52761780497506905, -1.784033869580059939, -1.500000000000002220 ) ) ;
#1210=CARTESIAN_POINT ( 'NONE',  ( -40.49855218390116818, -24.15503026093912453, -0.2815557561904605821 ) ) ;
#1212=CARTESIAN_POINT ( 'NONE',  ( 5.194767643164344584, 22.50260600399833422, -1.500000000000002220 ) ) ;
#1214=CARTESIAN_POINT ( 'NONE',  ( -93.50527755429412480, -24.65952944569305316, 1.056160979905699904 ) ) ;
#1215=PLANE ( 'NONE',  #21468 ) ;
#1218=CARTESIAN_POINT ( 'NONE',  ( -111.2413225215033634, -25.29823881010014475, 3.153768976815904956 ) ) ;
#1219=B_SPLINE_CURVE_WITH_KNOTS ( 'NONE', 3,
 ( #9722, #63526, #40677, #41177 ),
 .UNSPECIFIED., .F., .F.,
 ( 4, 4 ),
 ( 1.387778780781445676E-17, 9.999999999996123101E-05 ),
 .UNSPECIFIED. ) ;
#1220=CARTESIAN_POINT ( 'NONE',  ( -124.5562042904834072, -23.48786465467241769, 11.44779295918253759 ) ) ;
#1221=CARTESIAN_POINT ( 'NONE',  ( -114.6266390397259869, -24.15620529776629155, 10.23563542870659404 ) ) ;
#1222=CARTESIAN_POINT ( 'NONE',  ( -4.359361796094493258, -19.42695174060331809, 11.49999999999998934 ) ) ;
#1224=CARTESIAN_POINT ( 'NONE',  ( -75.50249853208187290, -24.40133493613049964, 9.663955038902805939 ) ) ;
#1225=CARTESIAN_POINT ( 'NONE',  ( -18.99895575154661742, -5.639348582513488140, -1.500000000000002220 ) ) ;
#1228=CARTESIAN_POINT ( 'NONE',  ( -56.59864057370428014, -23.96119346886880663, -0.6495511937832126881 ) ) ;
#1230=CARTESIAN_POINT ( 'NONE',  ( -95.62287095715005592, -24.99132157543084531, 2.256160258750667502 ) ) ;
#1231=CARTESIAN_POINT ( 'NONE',  ( -15.76495264167062160, -13.51897010167481739, 11.49999999999999645 ) ) ;
#1233=CARTESIAN_POINT ( 'NONE',  ( -110.6228709571500559, -29.50250243563736774, 8.947779886222136270 ) ) ;
#1234=B_SPLINE_CURVE_WITH_KNOTS ( 'NONE', 3,
 ( #27033, #90425, #29019, #82803, #35152, #50878, #35649, #97041, #43758, #51874, #83302, #89928, #28519, #66124 ),
 .UNSPECIFIED., .F., .F.,
 ( 4, 2, 2, 2, 2, 2, 4 ),
 ( 1.398578778534940505E-17, 0.0002750759563669337307, 0.0005501519127338534753, 0.001100303825467730586, 0.001650455738201607805, 0.001925531694568536874, 0.002200607650935465943 ),
 .UNSPECIFIED. ) ;
#1235=ADVANCED_FACE ( 'NONE', ( #95443 ), #65029, .F. ) ;
#1236=CARTESIAN_POINT ( 'NONE',  ( -120.5228709571500616, -29.50249982740957577, 7.747779886224967605 ) ) ;
#1237=CARTESIAN_POINT ( 'NONE',  ( -19.53289989604362376, -11.71160353944097920, 11.49999999999999645 ) ) ;
#1238=ORIENTED_EDGE ( 'NONE', *, *, #52855, .T. ) ;
#1239=B_SPLINE_SURFACE_WITH_KNOTS ( 'NONE', 3, 3, ( 
 ( #18580, #86599, #70890, #19081 ),
 ( #39927, #95717, #40930, #87609 ),
 ( #17591, #87099, #94204, #25699 ),
 ( #63287, #71892, #48049, #79985 ),
 ( #2886, #78979, #55673, #26707 ),
 ( #10474, #24689, #49057, #1872 ),
 ( #41432, #32314, #9476, #72391 ) ),
 .UNSPECIFIED., .F., .F., .F.,
 ( 4, 3, 4 ),
 ( 4, 4 ),
 ( 0.7945040050992242531, 0.8970133687736503436, 0.9995227324480764342 ),
 ( 0.6696641681890944664, 0.6709860541624589336 ),
 .UNSPECIFIED. ) ;
#1240=CARTESIAN_POINT ( 'NONE',  ( -83.62287095715002749, -24.51387760970723306, 9.387446482453402297 ) ) ;
#1243=ORIENTED_EDGE ( 'NONE', *, *, #92389, .F. ) ;
#1244=CARTESIAN_POINT ( 'NONE',  ( 7.037473118728134303, -18.94123407977296480, 11.49999999999998934 ) ) ;
#1245=DIRECTION ( 'NONE',  ( 0.000000000000000000, 0.9999999999976377785, 2.173523156925979975E-06 ) ) ;
#1247=CARTESIAN_POINT ( 'NONE',  ( -40.41683116089613748, -25.30532407203700984, 5.082404393492757855 ) ) ;
#1248=EDGE_CURVE ( 'NONE', #92355, #38340, #26668, .T. ) ;
#1249=ORIENTED_EDGE ( 'NONE', *, *, #89542, .F. ) ;
#1250=CARTESIAN_POINT ( 'NONE',  ( -40.52287095715006870, -23.48786465467241058, 11.44779295918255180 ) ) ;
#1251=CARTESIAN_POINT ( 'NONE',  ( -9.675568039816649701, -20.77828039667204862, -1.500000000000002220 ) ) ;
#1252=CARTESIAN_POINT ( 'NONE',  ( -29.47549908493335735, -24.57252240364413609, 1.056161296257513094 ) ) ;
#1253=EDGE_CURVE ( 'NONE', #19743, #19988, #14617, .T. ) ;
#1254=CARTESIAN_POINT ( 'NONE',  ( -15.89961544564849305, 12.09337254111102844, -1.500000000000002220 ) ) ;
#1255=CARTESIAN_POINT ( 'NONE',  ( -102.6228709571500559, -29.50248528299804818, 1.056150453629042030 ) ) ;
#1256=CARTESIAN_POINT ( 'NONE',  ( -5.413507703253908510, 20.27406835261982465, 11.49999999999999645 ) ) ;
#1257=CARTESIAN_POINT ( 'NONE',  ( -86.62287095715008434, -24.33927499327854704, 9.819080762295811837 ) ) ;
#1259=CARTESIAN_POINT ( 'NONE',  ( -5.411813039392390223, -21.34095290059367755, 11.49999999999998934 ) ) ;
#1263=CARTESIAN_POINT ( 'NONE',  ( -49.93954932203694597, -25.27344777607457260, 3.376895343913014713 ) ) ;
#1264=PLANE ( 'NONE',  #77022 ) ;
#1265=VERTEX_POINT ( 'NONE', #57408 ) ;
#1269=VERTEX_POINT ( 'NONE', #10209 ) ;
#1271=PLANE ( 'NONE',  #61 ) ;
#1273=CARTESIAN_POINT ( 'NONE',  ( -17.80769721941407369, -10.09151516499986734, -1.500000000000002220 ) ) ;
#1274=ORIENTED_EDGE ( 'NONE', *, *, #9439, .F. ) ;
#1275=FACE_OUTER_BOUND ( 'NONE', #69418, .T. ) ;
#1276=B_SPLINE_CURVE_WITH_KNOTS ( 'NONE', 3,
 ( #3253, #3745, #71753, #24557 ),
 .UNSPECIFIED., .F., .F.,
 ( 4, 4 ),
 ( 0.3907790457512309579, 0.3997854770233464916 ),
 .UNSPECIFIED. ) ;
#1277=CARTESIAN_POINT ( 'NONE',  ( -44.57673861720984831, -24.65952944569304606, 1.056160979905693909 ) ) ;
#1278=DIRECTION ( 'NONE',  ( -3.773278334453079618E-23, 0.9999999999976377785, 2.173523156925979975E-06 ) ) ;
#1279=CARTESIAN_POINT ( 'NONE',  ( 21.63714550250683644, -5.416328558471028565, -1.500000000000002220 ) ) ;
#1281=CARTESIAN_POINT ( 'NONE',  ( -90.62287095715004170, -24.99156045073392818, 7.747789690856161648 ) ) ;
#1283=CARTESIAN_POINT ( 'NONE',  ( -29.52587214738113275, -25.05018694314834349, 2.947979682295396753 ) ) ;
#1285=CARTESIAN_POINT ( 'NONE',  ( 9.770152518076534065, 18.40777400073588410, -1.500000000000002220 ) ) ;
#1286=ORIENTED_EDGE ( 'NONE', *, *, #25325, .T. ) ;
#1288=EDGE_LOOP ( 'NONE', ( #1431, #4389, #68582, #86609 ) ) ;
#1290=CARTESIAN_POINT ( 'NONE',  ( -51.45055690290539019, -25.25854447648429257, 6.541366898730298196 ) ) ;
#1291=CARTESIAN_POINT ( 'NONE',  ( 20.48634023128459347, 4.603634630958829632, -1.500000000000002220 ) ) ;
#1292=ORIENTED_EDGE ( 'NONE', *, *, #53692, .T. ) ;
#1293=CARTESIAN_POINT ( 'NONE',  ( -93.62287095715005592, -24.66019654487199730, 8.947790411086124607 ) ) ;
#1294=CARTESIAN_POINT ( 'NONE',  ( -105.6228709571500559, -29.50247984919015209, -1.443849546365048253 ) ) ;
#1296=CARTESIAN_POINT ( 'NONE',  ( -86.59169610958005592, -24.15620529776628445, 10.23563542870660292 ) ) ;
#1297=CARTESIAN_POINT ( 'NONE',  ( -59.54289001521522096, -24.34968618360933235, 0.1864209137778795600 ) ) ;
#1299=CARTESIAN_POINT ( 'NONE',  ( 21.63176498729014341, 4.993826359924048219, 11.49999999999999645 ) ) ;
#1300=ORIENTED_EDGE ( 'NONE', *, *, #97309, .F. ) ;
#1303=ORIENTED_EDGE ( 'NONE', *, *, #28565, .F. ) ;
#1304=CARTESIAN_POINT ( 'NONE',  ( -18.74212433040710479, 12.77821124017617649, 11.49999999999998934 ) ) ;
#1307=VERTEX_POINT ( 'NONE', #33546 ) ;
#1311=CARTESIAN_POINT ( 'NONE',  ( 19.08902475966321788, 6.433202353099247262, -1.500000000000002220 ) ) ;
#1312=CARTESIAN_POINT ( 'NONE',  ( -80.62287095715004170, -23.48783264082478439, -1.443836473390065489 ) ) ;
#1315=CARTESIAN_POINT ( 'NONE',  ( -19.61019785865472542, -10.87575402790796453, -1.500000000000002220 ) ) ;
#1321=EDGE_CURVE ( 'NONE', #27358, #38179, #32770, .T. ) ;
#1323=CARTESIAN_POINT ( 'NONE',  ( -116.5228709571500332, -24.33927499327855415, 9.819080762295804732 ) ) ;
#1326=CARTESIAN_POINT ( 'NONE',  ( -63.92778996623335530, -24.47827083238275847, 0.5637492489085984548 ) ) ;
#1327=CARTESIAN_POINT ( 'NONE',  ( 3.528372621398383924, 19.26332229581237598, 11.49999999999998934 ) ) ;
#1328=CARTESIAN_POINT ( 'NONE',  ( -38.52287095715006870, -29.50250243563736774, 8.947779886222148704 ) ) ;
#1330=EDGE_CURVE ( 'NONE', #34031, #100041, #19461, .T. ) ;
#1331=CARTESIAN_POINT ( 'NONE',  ( 14.19067371521932230, 16.14321034643037578, -1.500000000000002220 ) ) ;
#1332=CARTESIAN_POINT ( 'NONE',  ( -102.5562042904833930, -23.48786465467241058, 11.44779295918254114 ) ) ;
#1334=CARTESIAN_POINT ( 'NONE',  ( -113.5228709571500616, -24.35013146730205236, 9.818937971375095941 ) ) ;
#1335=CARTESIAN_POINT ( 'NONE',  ( -111.6228709571500559, -24.65952944569304606, 1.056160979905703901 ) ) ;
#1336=CARTESIAN_POINT ( 'NONE',  ( -2.941484630304247450, -22.72858670154147376, -1.500000000000002220 ) ) ;
#1337=VECTOR ( 'NONE', #93193, 1000.000000000000114 ) ;
#1339=DIRECTION ( 'NONE',  ( -0.000000000000000000, 2.173523156925979552E-06, -0.9999999999976378895 ) ) ;
#1340=CARTESIAN_POINT ( 'NONE',  ( -42.52287095715005449, -23.96127896942123670, -0.6493128930941061139 ) ) ;
#1341=CARTESIAN_POINT ( 'NONE',  ( 19.36564117097816862, 5.170944958934900804, 11.49999999999999645 ) ) ;
#1342=DIRECTION ( 'NONE',  ( 0.000000000000000000, -0.9999999999976377785, -2.173523156925979128E-06 ) ) ;
#1346=CARTESIAN_POINT ( 'NONE',  ( -71.62287095715005592, -29.50250243563736774, 8.947779886222143375 ) ) ;
#1347=VERTEX_POINT ( 'NONE', #1602 ) ;
#1348=CARTESIAN_POINT ( 'NONE',  ( -50.62287095715008434, -24.52323809116984421, 9.355190652339420154 ) ) ;
#1349=ADVANCED_FACE ( 'NONE', ( #17313 ), #48278, .T. ) ;
#1350=CARTESIAN_POINT ( 'NONE',  ( -16.08361747308824263, -14.67194924222005170, 11.49999999999998934 ) ) ;
#1351=CARTESIAN_POINT ( 'NONE',  ( -65.62287095715005592, -23.47596703998600631, 11.44779298504227683 ) ) ;
#1352=CARTESIAN_POINT ( 'NONE',  ( 18.74904333037421011, -5.873301551693434597, -1.500000000000002220 ) ) ;
#1358=CARTESIAN_POINT ( 'NONE',  ( -91.59781932095023649, -23.73791477778911840, 11.05961554403170410 ) ) ;
#1360=CARTESIAN_POINT ( 'NONE',  ( -18.11865614447288664, 9.752654332028551920, 11.49999999999999645 ) ) ;
#1362=EDGE_CURVE ( 'NONE', #22913, #18521, #44812, .T. ) ;
#1363=CARTESIAN_POINT ( 'NONE',  ( -120.5888113947464291, -24.73486907724918638, 1.287355809206965684 ) ) ;
#1364=CARTESIAN_POINT ( 'NONE',  ( 15.43685675143394498, -16.52047792065556564, 11.49999999999999645 ) ) ;
#1367=CARTESIAN_POINT ( 'NONE',  ( -99.59758909298055585, -25.31296351044734649, 4.277504013324993970 ) ) ;
#1371=CARTESIAN_POINT ( 'NONE',  ( -26.05468383228075169, -24.61459909436555549, 7.311465941504138755 ) ) ;
#1374=EDGE_CURVE ( 'NONE', #83628, #62593, #21786, .T. ) ;
#1377=CARTESIAN_POINT ( 'NONE',  ( 21.82588152991271713, 6.770963248321698380, 11.49999999999998934 ) ) ;
#1378=CARTESIAN_POINT ( 'NONE',  ( -125.5895376238167245, -25.00158670708909625, 2.256160236439167299 ) ) ;
#1379=B_SPLINE_SURFACE_WITH_KNOTS ( 'NONE', 3, 1, ( 
 ( #63782, #7957 ),
 ( #94190, #86585 ),
 ( #55659, #38913 ),
 ( #9463, #24182 ),
 ( #55158, #48037 ),
 ( #71378, #1860 ),
 ( #48547, #32804 ),
 ( #94698, #42438 ),
 ( #50044, #10969 ),
 ( #96211, #80474 ),
 ( #79974, #2873 ),
 ( #34309, #73372 ),
 ( #49545, #25688 ),
 ( #33295, #64281 ),
 ( #18077, #19570 ),
 ( #72877, #49045 ),
 ( #41934, #2364 ),
 ( #95205, #65287 ),
 ( #56658, #72378 ) ),
 .UNSPECIFIED., .F., .F., .F.,
 ( 4, 1, 1, 1, 1, 1, 1, 1, 1, 1, 1, 1, 1, 1, 1, 1, 4 ),
 ( 2, 2 ),
 ( 0.000000000000000000, 0.06796237149444751824, 0.1332834028675206339, 0.1978352977570501381, 0.2608919865309831110, 0.3233765044831737323, 0.3863500754690828431, 0.4496377310517088999, 0.5147953269783526187, 0.5792399132410260831, 0.6418141777582863083, 0.7013585647860591799, 0.7607267659857173125, 0.8192220679243865655, 0.8787161693846299304, 0.9381473540533079580, 1.000000000000000000 ),
 ( 0.000000000000000000, 1.000000000000000000 ),
 .UNSPECIFIED. ) ;
#1380=CARTESIAN_POINT ( 'NONE',  ( -96.62764832958193040, -24.34968618360933945, 0.1864209137778869152 ) ) ;
#1382=CARTESIAN_POINT ( 'NONE',  ( -3.368041826647835357, -22.21310627845187824, 11.49999999999999645 ) ) ;
#1383=ORIENTED_EDGE ( 'NONE', *, *, #3275, .F. ) ;
#1384=CARTESIAN_POINT ( 'NONE',  ( -43.64731547651398813, -23.96119346886880663, -0.6495511937831988103 ) ) ;
#1385=CARTESIAN_POINT ( 'NONE',  ( -3.149188516569510377, 21.71089317892358395, 11.49999999999998934 ) ) ;
#1387=CARTESIAN_POINT ( 'NONE',  ( -44.49312653990953237, -24.35071581493543036, 9.817618358456025263 ) ) ;
#1388=DIRECTION ( 'NONE',  ( 1.000000000000000000, 3.773278334444167608E-23, 8.201307833595939069E-29 ) ) ;
#1390=CARTESIAN_POINT ( 'NONE',  ( -48.51405841811074993, -23.73791477778911840, 11.05961554403170766 ) ) ;
#1393=CARTESIAN_POINT ( 'NONE',  ( -3.437008290023895185, 20.19323497536227663, -1.500000000000002220 ) ) ;
#1395=ORIENTED_EDGE ( 'NONE', *, *, #76896, .F. ) ;
#1396=ORIENTED_EDGE ( 'NONE', *, *, #6681, .T. ) ;
#1398=CARTESIAN_POINT ( 'NONE',  ( -5.126879528927636542, -22.49243673399587351, -1.500000000000002220 ) ) ;
#1399=CARTESIAN_POINT ( 'NONE',  ( -82.52287095715007581, -24.33832256527049154, 0.1851278514138627596 ) ) ;
#1400=CARTESIAN_POINT ( 'NONE',  ( -15.67655817637044890, 12.86142704545212290, -1.500000000000002220 ) ) ;
#1401=ORIENTED_EDGE ( 'NONE', *, *, #73281, .T. ) ;
#1403=AXIS2_PLACEMENT_3D ( 'NONE', #43039, #41540, #73479 ) ;
#1404=CARTESIAN_POINT ( 'NONE',  ( -92.59430350763778961, -23.96119346886881374, -0.6495511937831873750 ) ) ;
#1407=CARTESIAN_POINT ( 'NONE',  ( 19.88731969966643476, 8.162773808193900749, 11.49999999999999645 ) ) ;
#1409=CARTESIAN_POINT ( 'NONE',  ( -75.56671859597047103, -23.48783264082477018, -1.443836473390089914 ) ) ;
#1410=CARTESIAN_POINT ( 'NONE',  ( -104.6228709571500985, -23.94994826722515668, -0.6494450866351708651 ) ) ;
#1412=CARTESIAN_POINT ( 'NONE',  ( 18.78520451414993531, -8.817701518030307994, 11.49999999999998934 ) ) ;
#1413=ORIENTED_EDGE ( 'NONE', *, *, #87246, .T. ) ;
#1414=CARTESIAN_POINT ( 'NONE',  ( -125.5890728391331521, -24.83618233451450763, 1.606449574219537046 ) ) ;
#1416=CARTESIAN_POINT ( 'NONE',  ( -111.5955154881536799, -23.48786465467241769, 11.44779295918254114 ) ) ;
#1417=DIRECTION ( 'NONE',  ( -3.773278334444167608E-23, 1.000000000000000000, 0.000000000000000000 ) ) ;
#1418=VERTEX_POINT ( 'NONE', #67501 ) ;
#1419=ORIENTED_EDGE ( 'NONE', *, *, #34775, .T. ) ;
#1420=DIRECTION ( 'NONE',  ( -3.773278334444167608E-23, 1.000000000000000000, 0.000000000000000000 ) ) ;
#1421=VECTOR ( 'NONE', #80102, 1000.000000000000114 ) ;
#1423=CARTESIAN_POINT ( 'NONE',  ( -27.79921587522528625, -24.62298669958403252, 1.630323915293501624 ) ) ;
#1424=CARTESIAN_POINT ( 'NONE',  ( -20.26759042640731323, -8.618136523154847239, 11.49999999999999645 ) ) ;
#1425=CARTESIAN_POINT ( 'NONE',  ( -89.54580542116907793, -24.51419770103157703, 9.386484678747176957 ) ) ;
#1426=CARTESIAN_POINT ( 'NONE',  ( -8.633696204196466439, -20.85254729778420923, 11.49999999999998934 ) ) ;
#1427=CARTESIAN_POINT ( 'NONE',  ( 14.09988904737591575, 15.55221489148801872, 11.49999999999998934 ) ) ;
#1429=ORIENTED_EDGE ( 'NONE', *, *, #54413, .F. ) ;
#1430=AXIS2_PLACEMENT_3D ( 'NONE', #10725, #87335, #58409 ) ;
#1431=ORIENTED_EDGE ( 'NONE', *, *, #95584, .T. ) ;
#1432=DIRECTION ( 'NONE',  ( -1.000000000000000000, -3.773278334444166432E-23, -8.201307841325785021E-29 ) ) ;
#1433=B_SPLINE_CURVE_WITH_KNOTS ( 'NONE', 3,
 ( #60116, #98643, #43878, #4817, #91040, #67729 ),
 .UNSPECIFIED., .F., .F.,
 ( 4, 2, 4 ),
 ( 1.570755371633974110E-05, 0.001396183895866087103, 0.002776660238015834711 ),
 .UNSPECIFIED. ) ;
#1435=EDGE_LOOP ( 'NONE', ( #98396, #57347, #37572, #98327 ) ) ;
#1436=CARTESIAN_POINT ( 'NONE',  ( -8.144517828999388698, 19.50133175306300970, 11.49999999999998934 ) ) ;
#1437=CARTESIAN_POINT ( 'NONE',  ( -117.6228709571500559, -23.47593901973091235, -1.443836447538997536 ) ) ;
#1438=EDGE_CURVE ( 'NONE', #65965, #61548, #13186, .T. ) ;
#1439=CARTESIAN_POINT ( 'NONE',  ( -51.78109907783319699, -25.03148574646757396, 6.793045521090960825 ) ) ;
#1440=CARTESIAN_POINT ( 'NONE',  ( -49.50841769935764347, -25.26288593538659910, 3.984447754961206734 ) ) ;
#1441=CARTESIAN_POINT ( 'NONE',  ( -109.5895376238167245, -24.66019654487200441, 8.947790411086117501 ) ) ;
#1442=CARTESIAN_POINT ( 'NONE',  ( -111.9545732713065291, -25.06732945298220372, 7.447791367849804445 ) ) ;
#1443=CARTESIAN_POINT ( 'NONE',  ( 18.30470771955606679, 12.64531542519679697, -1.500000000000002220 ) ) ;
#1444=EDGE_CURVE ( 'NONE', #81452, #60342, #47333, .T. ) ;
#1445=CARTESIAN_POINT ( 'NONE',  ( -74.62287095715005592, -24.50321055353806443, 9.387540953477538253 ) ) ;
#1446=EDGE_CURVE ( 'NONE', #62104, #68431, #6168, .T. ) ;
#1447=ORIENTED_EDGE ( 'NONE', *, *, #39669, .T. ) ;
#1449=CARTESIAN_POINT ( 'NONE',  ( -58.62287095715007013, -23.47596703998600276, 11.44779298504227683 ) ) ;
#1454=CARTESIAN_POINT ( 'NONE',  ( -4.154358412494840280, 19.03220294597612039, -1.500000000000002220 ) ) ;
#1455=CARTESIAN_POINT ( 'NONE',  ( -17.32345979880200204, -12.59856583755568415, -1.500000000000002220 ) ) ;
#1457=CARTESIAN_POINT ( 'NONE',  ( -60.63095941313405746, -24.73531770709804078, 8.716586749031112191 ) ) ;
#1458=CARTESIAN_POINT ( 'NONE',  ( -51.59327120193346872, -24.15543982623907127, -0.2315651400026664530 ) ) ;
#1459=CARTESIAN_POINT ( 'NONE',  ( -101.2457357660222641, -25.18440107031529251, 3.734961042421667710 ) ) ;
#1460=CARTESIAN_POINT ( 'NONE',  ( -9.471985145535571249, 20.67137392225973258, -1.500000000000002220 ) ) ;
#1461=CARTESIAN_POINT ( 'NONE',  ( -98.92287095715008149, -23.47596703998600631, 11.44779298504227860 ) ) ;
#1462=FACE_OUTER_BOUND ( 'NONE', #27362, .T. ) ;
#1463=CARTESIAN_POINT ( 'NONE',  ( 11.68167410197319001, -16.05257874518773065, 11.49999999999999645 ) ) ;
#1464=CARTESIAN_POINT ( 'NONE',  ( -84.52287095715004739, -24.34917612406836795, 0.1852690917426538242 ) ) ;
#1470=CARTESIAN_POINT ( 'NONE',  ( -49.28481975526113956, -25.23807781832389807, 6.283675252660968269 ) ) ;
#1471=CARTESIAN_POINT ( 'NONE',  ( -80.52287095715007581, -24.82576562948888821, 8.398263436605416743 ) ) ;
#1472=CARTESIAN_POINT ( 'NONE',  ( -71.52287095715009002, -23.72773821059536559, 11.05748984161097326 ) ) ;
#1473=CARTESIAN_POINT ( 'NONE',  ( -11.49108604648090548, 18.38894055434275643, -1.500000000000002220 ) ) ;
#1474=CARTESIAN_POINT ( 'NONE',  ( -32.62287095715005592, -24.66019654487199020, 8.947790411086137041 ) ) ;
#1475=VECTOR ( 'NONE', #35471, 1000.000000000000000 ) ;
#1476=CARTESIAN_POINT ( 'NONE',  ( 1.133552453683672745, -19.47370032599940615, -1.500000000000002220 ) ) ;
#1477=CARTESIAN_POINT ( 'NONE',  ( -55.53716315595536912, -24.63419186844611986, 9.035850630976923981 ) ) ;
#1478=ADVANCED_FACE ( 'NONE', ( #28924 ), #21793, .T. ) ;
#1480=B_SPLINE_CURVE_WITH_KNOTS ( 'NONE', 3,
 ( #52244, #61362, #37009, #85177 ),
 .UNSPECIFIED., .F., .F.,
 ( 4, 4 ),
 ( 0.000000000000000000, 9.999999999998900014E-05 ),
 .UNSPECIFIED. ) ;
#1482=CARTESIAN_POINT ( 'NONE',  ( 20.11976772532220181, -3.360927329567881205, 11.49999999999999645 ) ) ;
#1483=CARTESIAN_POINT ( 'NONE',  ( -93.52287095715006160, -24.65952944569304606, 1.056160979905700570 ) ) ;
#1484=DIRECTION ( 'NONE',  ( 0.000000000000000000, 2.173523156925980399E-06, -0.9999999999976378895 ) ) ;
#1485=ORIENTED_EDGE ( 'NONE', *, *, #77012, .T. ) ;
#1486=CARTESIAN_POINT ( 'NONE',  ( -78.94303308397306296, -25.26642230834568537, 5.977536689587218177 ) ) ;
#1488=CARTESIAN_POINT ( 'NONE',  ( -114.2228709571500787, -23.47593901973090524, -1.443836447538996426 ) ) ;
#1489=VECTOR ( 'NONE', #85606, 1000.000000000000114 ) ;
#1490=LINE ( 'NONE', #39036, #63525 ) ;
#1491=CARTESIAN_POINT ( 'NONE',  ( -129.5562042904833504, -23.48783264082478794, -1.443836473390056385 ) ) ;
#1492=CARTESIAN_POINT ( 'NONE',  ( 15.17442925503088169, 13.16703847180013831, 11.49999999999998934 ) ) ;
#1494=ORIENTED_EDGE ( 'NONE', *, *, #83961, .F. ) ;
#1496=ADVANCED_FACE ( 'NONE', ( #91321 ), #60400, .F. ) ;
#1497=CARTESIAN_POINT ( 'NONE',  ( 21.44032754495887261, 8.191337786432022483, 11.49999999999999645 ) ) ;
#1498=CARTESIAN_POINT ( 'NONE',  ( -18.45961786539058380, -13.25243217869837231, 11.49999999999998934 ) ) ;
#1501=CARTESIAN_POINT ( 'NONE',  ( -75.62287095715009855, -24.92604778743018556, 8.074972756849360778 ) ) ;
#1502=CARTESIAN_POINT ( 'NONE',  ( -38.48524076036703434, -24.51419770103157347, 9.386484678747176957 ) ) ;
#1503=CARTESIAN_POINT ( 'NONE',  ( -30.57287095715006231, -25.30570897125571861, 4.442708032791744088 ) ) ;
#1504=EDGE_CURVE ( 'NONE', #11582, #65087, #6086, .T. ) ;
#1507=CARTESIAN_POINT ( 'NONE',  ( -49.46084499080052410, -25.31520542434502730, 5.106140872684356680 ) ) ;
#1508=CARTESIAN_POINT ( 'NONE',  ( -54.52287095715006870, -24.64898659630367916, 1.056161002820821038 ) ) ;
#1509=CARTESIAN_POINT ( 'NONE',  ( -81.62287095715005592, -23.47593901973091235, -1.443836447539004642 ) ) ;
#1511=CARTESIAN_POINT ( 'NONE',  ( -17.41452279269062586, 10.58001483151439004, -1.500000000000002220 ) ) ;
#1513=CARTESIAN_POINT ( 'NONE',  ( -19.06187107478486098, -12.82570580458313003, 11.49999999999998934 ) ) ;
#1514=CARTESIAN_POINT ( 'NONE',  ( -53.62287095715004881, -23.48786465467241058, 11.44779295918255002 ) ) ;
#1515=ORIENTED_EDGE ( 'NONE', *, *, #56665, .F. ) ;
#1516=LINE ( 'NONE', #93849, #47711 ) ;
#1517=CARTESIAN_POINT ( 'NONE',  ( -99.62287095715005592, -24.64965695001468404, 8.947790433994178727 ) ) ;
#1518=CARTESIAN_POINT ( 'NONE',  ( -96.62287095715005592, -24.64898659630368272, 1.056161002820829697 ) ) ;
#1519=CARTESIAN_POINT ( 'NONE',  ( 21.14028111218437900, -2.610574537768086234, 11.49999999999999645 ) ) ;
#1520=ORIENTED_EDGE ( 'NONE', *, *, #92917, .T. ) ;
#1522=CARTESIAN_POINT ( 'NONE',  ( -17.05807961832342912, 14.25954964135033265, 11.49999999999998934 ) ) ;
#1523=B_SPLINE_CURVE_WITH_KNOTS ( 'NONE', 3,
 ( #7775, #8278, #64095, #47847, #24495, #24993, #31608, #39219, #62077, #86401, #17390, #16886, #48353, #40730, #85901, #70176, #79282, #9776, #33117, #54457, #71688, #56476, #95013, #38721, #78270, #2185 ),
 .UNSPECIFIED., .F., .F.,
 ( 4, 2, 2, 2, 2, 2, 2, 2, 2, 2, 2, 2, 4 ),
 ( 1.045815803166493187E-05, 0.001697191910848542444, 0.002540558787256983614, 0.003383925663665425000, 0.004227292540073865519, 0.005070659416482306038, 0.006757393169299188811, 0.007600760045707628462, 0.008444126922116070716, 0.01013086067493295175, 0.01097422755134139054, 0.01181759442774982932, 0.01350432818056671036 ),
 .UNSPECIFIED. ) ;
#1524=CARTESIAN_POINT ( 'NONE',  ( 10.61356161029474521, 17.70173163822984819, 11.49999999999998934 ) ) ;
#1525=ORIENTED_EDGE ( 'NONE', *, *, #47678, .F. ) ;
#1527=CARTESIAN_POINT ( 'NONE',  ( -95.54445401090212897, -24.83644354573579349, 8.397322867130096569 ) ) ;
#1529=CARTESIAN_POINT ( 'NONE',  ( -95.52287095715004739, -24.51163499207179797, 0.6490370598555494919 ) ) ;
#1532=CARTESIAN_POINT ( 'NONE',  ( -58.59839921736052304, -23.96169478059713143, 10.65365249895718058 ) ) ;
#1534=CARTESIAN_POINT ( 'NONE',  ( -20.60679684081203789, -3.318877370925724879, -1.500000000000002220 ) ) ;
#1535=CARTESIAN_POINT ( 'NONE',  ( -21.01659442711627790, -5.882202039844940167, 11.49999999999999645 ) ) ;
#1538=CARTESIAN_POINT ( 'NONE',  ( -17.89120377161202313, 13.61666483413312712, -1.500000000000002220 ) ) ;
#1540=CARTESIAN_POINT ( 'NONE',  ( -44.52287095715006160, -24.64898659630367916, 1.056161002820819261 ) ) ;
#1541=CARTESIAN_POINT ( 'NONE',  ( -53.62287095715005592, -24.64898659630528499, 1.056161002820821038 ) ) ;
#1543=ORIENTED_EDGE ( 'NONE', *, *, #40430, .T. ) ;
#1544=VECTOR ( 'NONE', #59527, 1000.000000000000114 ) ;
#1546=AXIS2_PLACEMENT_3D ( 'NONE', #67638, #58037, #97074 ) ;
#1551=CARTESIAN_POINT ( 'NONE',  ( 10.55508701655855575, -18.62573008410804221, -1.500000000000002220 ) ) ;
#1552=CARTESIAN_POINT ( 'NONE',  ( 5.437191932089902480, -21.69250089042843754, 11.49999999999999645 ) ) ;
#1554=CARTESIAN_POINT ( 'NONE',  ( -43.62287095715004881, -24.64898659630367206, 1.056161002820819261 ) ) ;
#1555=CARTESIAN_POINT ( 'NONE',  ( 16.02493003730957000, -13.65669227992738577, -1.500000000000002220 ) ) ;
#1556=CARTESIAN_POINT ( 'NONE',  ( -30.43720465287918131, -24.37652013707292298, 9.702671485061733492 ) ) ;
#1558=CARTESIAN_POINT ( 'NONE',  ( -19.24466553037914807, -5.328869878250761971, -1.500000000000002220 ) ) ;
#1561=CARTESIAN_POINT ( 'NONE',  ( -19.65368394218270254, -10.04821906498216499, -1.500000000000002220 ) ) ;
#1562=DIRECTION ( 'NONE',  ( -3.773278334444166432E-23, 1.000000000000000000, 0.000000000000000000 ) ) ;
#1564=CARTESIAN_POINT ( 'NONE',  ( -65.65276306346875401, -23.85049219812685806, 10.88485053497527311 ) ) ;
#1567=CARTESIAN_POINT ( 'NONE',  ( 8.688630223215852766, -18.96179456382524364, 11.49999999999999645 ) ) ;
#1570=ADVANCED_FACE ( 'NONE', ( #53272 ), #23893, .T. ) ;
#1571=PLANE ( 'NONE',  #92693 ) ;
#1572=CARTESIAN_POINT ( 'NONE',  ( -38.62287095715007013, -23.73934037231757088, 11.05740245334329863 ) ) ;
#1573=CARTESIAN_POINT ( 'NONE',  ( -9.236746577462426444, 19.23066362772381055, 11.49999999999998934 ) ) ;
#1574=PLANE ( 'NONE',  #33711 ) ;
#1576=CARTESIAN_POINT ( 'NONE',  ( -80.52287095715004739, -25.00182538069145366, 7.747789668545104647 ) ) ;
#1577=CARTESIAN_POINT ( 'NONE',  ( -96.52287095715001897, -24.51387760970724727, 9.387446482453407626 ) ) ;
#1579=CARTESIAN_POINT ( 'NONE',  ( -10.06026007034034464, -20.14757889648583244, -1.500000000000002220 ) ) ;
#1582=LINE ( 'NONE', #71593, #74186 ) ;
#1583=CARTESIAN_POINT ( 'NONE',  ( -31.56131522125139810, -23.73791477778911130, 11.05961554403171299 ) ) ;
#1584=CARTESIAN_POINT ( 'NONE',  ( 15.21843288076463629, 12.49332292251147614, 11.49999999999999645 ) ) ;
#1586=DIRECTION ( 'NONE',  ( -3.773278334453079618E-23, 0.9999999999976377785, 2.173523156925979975E-06 ) ) ;
#1587=EDGE_CURVE ( 'NONE', #11601, #66619, #27923, .T. ) ;
#1591=CARTESIAN_POINT ( 'NONE',  ( -61.52287095715006160, -24.66019654487199730, 8.947790411086121054 ) ) ;
#1593=CARTESIAN_POINT ( 'NONE',  ( -5.448126336921106372, -18.99418723138115084, 11.49999999999998934 ) ) ;
#1595=CARTESIAN_POINT ( 'NONE',  ( 9.409760114191467295, 17.86087837679851020, 11.49999999999999645 ) ) ;
#1597=VECTOR ( 'NONE', #80561, 1000.000000000000114 ) ;
#1598=VERTEX_POINT ( 'NONE', #24310 ) ;
#1599=CARTESIAN_POINT ( 'NONE',  ( -48.62287095715006302, -24.33927499327853994, 9.819080762295820719 ) ) ;
#1600=CARTESIAN_POINT ( 'NONE',  ( -69.86951118291817409, -25.29879079004132336, 5.410841093910524258 ) ) ;
#1601=CARTESIAN_POINT ( 'NONE',  ( -50.72512992191887804, -25.30333624419147043, 5.237440092667283054 ) ) ;
#1602=CARTESIAN_POINT ( 'NONE',  ( -71.20541289166536103, -25.30502758240210071, 4.885889971059796721 ) ) ;
#1603=AXIS2_PLACEMENT_3D ( 'NONE', #38165, #53914, #84847 ) ;
#1604=CARTESIAN_POINT ( 'NONE',  ( -41.62287095715006302, -24.66019654487199020, 8.947790411086135265 ) ) ;
#1605=CARTESIAN_POINT ( 'NONE',  ( -127.5228709571500616, -24.65952944569304606, 1.056160979905707675 ) ) ;
#1606=CARTESIAN_POINT ( 'NONE',  ( -20.00956492049148494, -0.6725752471728385640, -1.500000000000002220 ) ) ;
#1607=EDGE_CURVE ( 'NONE', #3816, #73248, #16945, .T. ) ;
#1608=CARTESIAN_POINT ( 'NONE',  ( -117.5562042904833788, -24.64898659630529210, 1.056161002820830142 ) ) ;
#1609=CARTESIAN_POINT ( 'NONE',  ( -116.5892947015510259, -24.35071581493544102, 9.817618358456021710 ) ) ;
#1610=ORIENTED_EDGE ( 'NONE', *, *, #18664, .F. ) ;
#1614=CARTESIAN_POINT ( 'NONE',  ( -109.4679719608024300, -25.18430259236162172, 3.778970299867911109 ) ) ;
#1615=CARTESIAN_POINT ( 'NONE',  ( -35.52469202473817234, -24.83618233451450052, 1.606449574219543708 ) ) ;
#1616=CARTESIAN_POINT ( 'NONE',  ( -28.62287095715004881, -23.80673410051091921, 10.65359467416498163 ) ) ;
#1618=PLANE ( 'NONE',  #35085 ) ;
#1620=B_SPLINE_CURVE_WITH_KNOTS ( 'NONE', 3,
 ( #19979, #10879, #50948, #54321, #30467, #23846, #8139, #76622, #7124, #20471, #59558, #99956, #31467, #51442, #98090, #54820 ),
 .UNSPECIFIED., .F., .F.,
 ( 4, 2, 2, 2, 2, 2, 2, 4 ),
 ( 0.000000000000000000, 0.0002054542984747955402, 0.0004109085969495910803, 0.0008218171938991786912, 0.001027271492373979002, 0.001232725790848779313, 0.001438180089323579623, 0.001643634387798379934 ),
 .UNSPECIFIED. ) ;
#1623=EDGE_CURVE ( 'NONE', #49734, #5271, #54777, .T. ) ;
#1624=CARTESIAN_POINT ( 'NONE',  ( -50.29888690743871393, -25.18523929458199007, 3.296129346514034442 ) ) ;
#1625=ORIENTED_EDGE ( 'NONE', *, *, #62565, .T. ) ;
#1626=CARTESIAN_POINT ( 'NONE',  ( 9.679018533540549640, -17.85022214266596308, 11.49999999999998934 ) ) ;
#1628=CARTESIAN_POINT ( 'NONE',  ( -28.52287095715005805, -24.49893655963190042, 1.056161680022248195 ) ) ;
#1630=CARTESIAN_POINT ( 'NONE',  ( -59.59827874889279542, -23.96169478059713143, 10.65365249895718769 ) ) ;
#1632=CARTESIAN_POINT ( 'NONE',  ( -81.62287095715008434, -24.51283580621364777, 0.6167428607019832532 ) ) ;
#1633=CARTESIAN_POINT ( 'NONE',  ( -10.68008619461380704, -17.10268970254769982, -1.500000000000002220 ) ) ;
#1634=CARTESIAN_POINT ( 'NONE',  ( 12.34367313097222763, -17.18290682204727915, 11.49999999999999645 ) ) ;
#1635=CARTESIAN_POINT ( 'NONE',  ( 4.116201370682176730, 21.75534844777131838, 11.49999999999998934 ) ) ;
#1636=CARTESIAN_POINT ( 'NONE',  ( -9.016818060619870678, -18.48156098877705844, 11.49999999999998934 ) ) ;
#1641=CARTESIAN_POINT ( 'NONE',  ( -125.6228709571500559, -29.50249982740957577, 7.747779886224967605 ) ) ;
#1642=CARTESIAN_POINT ( 'NONE',  ( -129.6228709571500417, -23.47593901973091235, -1.443836447538995760 ) ) ;
#1643=VERTEX_POINT ( 'NONE', #40549 ) ;
#1644=ORIENTED_EDGE ( 'NONE', *, *, #20223, .T. ) ;
#1645=VERTEX_POINT ( 'NONE', #32930 ) ;
#1646=CARTESIAN_POINT ( 'NONE',  ( -111.2197402010974656, -25.17156514485315455, 3.135139282531213656 ) ) ;
#1649=CARTESIAN_POINT ( 'NONE',  ( -19.90621922972506397, 5.769413876575915978, -1.500000000000002220 ) ) ;
#1650=CARTESIAN_POINT ( 'NONE',  ( -10.61912389536305490, -18.88692380039396213, 11.49999999999999645 ) ) ;
#1651=ORIENTED_EDGE ( 'NONE', *, *, #34205, .T. ) ;
#1652=CARTESIAN_POINT ( 'NONE',  ( -99.01182976505512556, -25.29312185475552965, 5.556534405804150367 ) ) ;
#1654=CARTESIAN_POINT ( 'NONE',  ( 18.93296920960566965, -11.98514031388154599, -1.500000000000002220 ) ) ;
#1655=CARTESIAN_POINT ( 'NONE',  ( -47.63994631694639281, -24.15620529776627379, 10.23563542870660825 ) ) ;
#1656=CARTESIAN_POINT ( 'NONE',  ( -90.62287095715004170, -29.50248528299804818, 1.056150453629040253 ) ) ;
#1659=CARTESIAN_POINT ( 'NONE',  ( -35.58102505592412257, -24.73531770709095667, 8.716586749053508498 ) ) ;
#1660=B_SPLINE_CURVE_WITH_KNOTS ( 'NONE', 3,
 ( #20022, #35264, #58593, #60106 ),
 .UNSPECIFIED., .F., .F.,
 ( 4, 4 ),
 ( 0.000000000000000000, 9.999999999998897304E-05 ),
 .UNSPECIFIED. ) ;
#1662=ORIENTED_EDGE ( 'NONE', *, *, #54377, .T. ) ;
#1664=CARTESIAN_POINT ( 'NONE',  ( -43.52287095715006160, -23.47596703998600631, 11.44779298504229281 ) ) ;
#1666=DIRECTION ( 'NONE',  ( 0.000000000000000000, -2.173523156925980399E-06, 0.9999999999976378895 ) ) ;
#1667=CARTESIAN_POINT ( 'NONE',  ( -14.68016216564755894, -15.32010671487267572, -1.500000000000002220 ) ) ;
#1669=CARTESIAN_POINT ( 'NONE',  ( -50.54317153895161141, -24.40034930558990922, 0.3402023900116070698 ) ) ;
#1670=CARTESIAN_POINT ( 'NONE',  ( -21.69466673205137752, 2.402554924997643226, 11.49999999999998934 ) ) ;
#1671=CARTESIAN_POINT ( 'NONE',  ( -103.5909352260227934, -24.15620529776628445, 10.23563542870660292 ) ) ;
#1673=CARTESIAN_POINT ( 'NONE',  ( -43.62287095715004881, -24.64965695001467694, 8.947790433994187609 ) ) ;
#1675=CARTESIAN_POINT ( 'NONE',  ( 21.67628855941699939, -2.339797445609365756, -1.500000000000002220 ) ) ;
#1676=CARTESIAN_POINT ( 'NONE',  ( -95.62287095715005592, -25.00158670708909625, 2.256160236439165967 ) ) ;
#1679=CARTESIAN_POINT ( 'NONE',  ( -85.60107928363679264, -23.85049219812685450, 10.88485053497527133 ) ) ;
#1680=VERTEX_POINT ( 'NONE', #79596 ) ;
#1681=EDGE_LOOP ( 'NONE', ( #38410, #9651, #53587, #76774 ) ) ;
#1684=EDGE_CURVE ( 'NONE', #89148, #95501, #12089, .T. ) ;
#1685=DIRECTION ( 'NONE',  ( 0.000000000000000000, 2.173523156925980399E-06, -0.9999999999976378895 ) ) ;
#1687=CARTESIAN_POINT ( 'NONE',  ( -31.24388727629347784, -24.87219037989215309, 1.747789950310770779 ) ) ;
#1688=CARTESIAN_POINT ( 'NONE',  ( 20.00388196354723291, 7.160935007556333609, 11.49999999999998934 ) ) ;
#1690=EDGE_CURVE ( 'NONE', #80236, #95482, #59378, .T. ) ;
#1692=CARTESIAN_POINT ( 'NONE',  ( -44.62287095715004881, -23.48786465467240347, 11.44779295918255180 ) ) ;
#1693=FACE_OUTER_BOUND ( 'NONE', #83972, .T. ) ;
#1694=VECTOR ( 'NONE', #11060, 1000.000000000000114 ) ;
#1695=CARTESIAN_POINT ( 'NONE',  ( -4.539579955115475407, -18.87035741768621122, -1.500000000000002220 ) ) ;
#1696=B_SPLINE_CURVE_WITH_KNOTS ( 'NONE', 3,
 ( #29358, #69428, #100346, #60335, #30862, #91258 ),
 .UNSPECIFIED., .F., .F.,
 ( 4, 2, 4 ),
 ( 0.000000000000000000, 0.001380764517854765399, 0.002761529035709530365 ),
 .UNSPECIFIED. ) ;
#1697=CARTESIAN_POINT ( 'NONE',  ( -45.65169983139999488, -24.15503026093915651, -0.2815557561904415418 ) ) ;
#1699=AXIS2_PLACEMENT_3D ( 'NONE', #77975, #1388, #877 ) ;
#1700=CARTESIAN_POINT ( 'NONE',  ( 3.395600993332231532, 19.23619202488179525, 11.49999999999999645 ) ) ;
#1703=EDGE_CURVE ( 'NONE', #93093, #13092, #31505, .T. ) ;
#1704=ORIENTED_EDGE ( 'NONE', *, *, #4133, .T. ) ;
#1706=CARTESIAN_POINT ( 'NONE',  ( -89.62590769665170853, -24.51314013834317151, 0.6176544820404251679 ) ) ;
#1709=CARTESIAN_POINT ( 'NONE',  ( 18.74904333037421011, -5.873301551693434597, 11.49999999999998934 ) ) ;
#1712=CARTESIAN_POINT ( 'NONE',  ( 20.31487730549432413, -11.01532776123576518, -1.500000000000002220 ) ) ;
#1714=CARTESIAN_POINT ( 'NONE',  ( -125.5228709571500048, -24.63345952396256067, 9.038047939301506517 ) ) ;
#1716=CARTESIAN_POINT ( 'NONE',  ( -97.51896304891869249, -23.73791477778912196, 11.05961554403170410 ) ) ;
#1719=CARTESIAN_POINT ( 'NONE',  ( -129.5897716341975467, -24.15543982623907837, -0.2315651400026527140 ) ) ;
#1720=CARTESIAN_POINT ( 'NONE',  ( -114.6292354253845929, -23.73791477778912551, 11.05961554403169878 ) ) ;
#1721=CARTESIAN_POINT ( 'NONE',  ( 10.08953278062578462, 17.19620541797624824, 11.49999999999998934 ) ) ;
#1722=CARTESIAN_POINT ( 'NONE',  ( -75.58061766105404899, -24.92592662359561473, 8.075495903018000021 ) ) ;
#1723=CARTESIAN_POINT ( 'NONE',  ( 0.4224338394261131779, -19.80333402765648998, -1.500000000000002220 ) ) ;
#1725=CARTESIAN_POINT ( 'NONE',  ( -32.50560602629348494, -24.87219037988797865, 1.747789950295646877 ) ) ;
#1727=CARTESIAN_POINT ( 'NONE',  ( -51.51937581801175270, -25.24378128350642925, 6.324045589363499253 ) ) ;
#1728=CARTESIAN_POINT ( 'NONE',  ( -12.26507114386991226, -16.75673120704366426, 11.49999999999999645 ) ) ;
#1730=B_SPLINE_CURVE_WITH_KNOTS ( 'NONE', 3,
 ( #83994, #99211, #14477, #76368 ),
 .UNSPECIFIED., .F., .F.,
 ( 4, 4 ),
 ( 0.000000000000000000, 1.000000000000000000 ),
 .UNSPECIFIED. ) ;
#1732=ADVANCED_FACE ( 'NONE', ( #25814 ), #16617, .T. ) ;
#1733=CARTESIAN_POINT ( 'NONE',  ( -78.52287095715006160, -24.50321055353803956, 9.387540953477513384 ) ) ;
#1734=CARTESIAN_POINT ( 'NONE',  ( 0.8422786845129024424, 22.77647355728978340, 11.49999999999999645 ) ) ;
#1735=ORIENTED_EDGE ( 'NONE', *, *, #33658, .T. ) ;
#1736=CARTESIAN_POINT ( 'NONE',  ( -69.51616565026102990, -23.73766607897669445, -1.055555164236460008 ) ) ;
#1737=CARTESIAN_POINT ( 'NONE',  ( -89.52287095715006160, -23.47596703998600631, 11.44779298504228393 ) ) ;
#1739=CARTESIAN_POINT ( 'NONE',  ( -13.29518446780263119, -15.22762515321373478, -1.500000000000002220 ) ) ;
#1741=CARTESIAN_POINT ( 'NONE',  ( -110.5228709571500616, -23.48786465467242479, 11.44779295918253936 ) ) ;
#1743=CARTESIAN_POINT ( 'NONE',  ( -70.62287095715008434, -24.62285846362215835, 9.038163152653524435 ) ) ;
#1744=CARTESIAN_POINT ( 'NONE',  ( -21.95939045666098366, -6.591442671832903777, 11.49999999999998934 ) ) ;
#1746=VECTOR ( 'NONE', #69, 1000.000000000000114 ) ;
#1747=CARTESIAN_POINT ( 'NONE',  ( 19.86680303116296287, 2.261939200664708327, -1.500000000000002220 ) ) ;
#1748=CARTESIAN_POINT ( 'NONE',  ( -41.16195530322320195, -25.06433851276720048, 7.413582136084253094 ) ) ;
#1749=CARTESIAN_POINT ( 'NONE',  ( 14.09988904737591575, 15.55221489148801872, 11.49999999999999645 ) ) ;
#1750=VECTOR ( 'NONE', #88379, 1000.000000000000114 ) ;
#1751=CARTESIAN_POINT ( 'NONE',  ( -29.25979817829156815, -24.97066910737833112, 7.423742159896792536 ) ) ;
#1752=CARTESIAN_POINT ( 'NONE',  ( -124.5541598730913933, -24.65952944569305316, 1.056160979905707009 ) ) ;
#1753=CARTESIAN_POINT ( 'NONE',  ( -5.561696574893697509, -21.35426480686918538, -1.500000000000002220 ) ) ;
#1754=EDGE_CURVE ( 'NONE', #77182, #33349, #89562, .T. ) ;
#1757=CARTESIAN_POINT ( 'NONE',  ( -87.62287095715004170, -29.50250243563736774, 8.947779886222139822 ) ) ;
#1760=ORIENTED_EDGE ( 'NONE', *, *, #45425, .T. ) ;
#1761=CARTESIAN_POINT ( 'NONE',  ( -55.52287095715005449, -24.99156044556119483, 7.747789690856173195 ) ) ;
#1762=VERTEX_POINT ( 'NONE', #83454 ) ;
#1765=CARTESIAN_POINT ( 'NONE',  ( -47.62287095715004881, -29.50248528299804818, 1.056150453629033370 ) ) ;
#1767=CARTESIAN_POINT ( 'NONE',  ( 7.805751503010069037, -19.01748540344778959, -1.500000000000002220 ) ) ;
#1768=ORIENTED_EDGE ( 'NONE', *, *, #85282, .T. ) ;
#1770=EDGE_CURVE ( 'NONE', #62104, #35157, #76825, .T. ) ;
#1771=CARTESIAN_POINT ( 'NONE',  ( -33.62287095715004170, -24.51387760970722596, 9.387446482453418284 ) ) ;
#1773=CARTESIAN_POINT ( 'NONE',  ( -5.617636847906702258, 21.56867655435222630, 11.49999999999998934 ) ) ;
#1774=CARTESIAN_POINT ( 'NONE',  ( -0.07952141725841589681, -22.02053276243675484, 9.703205396196686650 ) ) ;
#1775=CARTESIAN_POINT ( 'NONE',  ( -26.97150317964156585, -24.62069184369231678, 8.115489842150878985 ) ) ;
#1776=VERTEX_POINT ( 'NONE', #37298 ) ;
#1778=B_SPLINE_CURVE_WITH_KNOTS ( 'NONE', 3,
 ( #96398, #43119, #74068, #4562 ),
 .UNSPECIFIED., .F., .F.,
 ( 4, 4 ),
 ( 0.000000000000000000, 0.0001000000000000028644 ),
 .UNSPECIFIED. ) ;
#1780=CARTESIAN_POINT ( 'NONE',  ( -8.730572200882948053, 18.91488879456464289, 11.49999999999998934 ) ) ;
#1783=EDGE_LOOP ( 'NONE', ( #71632, #89413, #23011, #37714 ) ) ;
#1784=B_SPLINE_CURVE_WITH_KNOTS ( 'NONE', 3,
 ( #86990, #80886, #56567, #41327, #71278, #48446 ),
 .UNSPECIFIED., .F., .F.,
 ( 4, 2, 4 ),
 ( 0.000000000000000000, 0.001380901958385388545, 0.002761803916770777089 ),
 .UNSPECIFIED. ) ;
#1785=ORIENTED_EDGE ( 'NONE', *, *, #5898, .F. ) ;
#1786=CARTESIAN_POINT ( 'NONE',  ( -69.11592688286732766, -25.03149225412030177, 6.884840797962249681 ) ) ;
#1787=CARTESIAN_POINT ( 'NONE',  ( 8.294003578737715543, -19.35633765900385939, -1.500000000000002220 ) ) ;
#1791=CARTESIAN_POINT ( 'NONE',  ( -97.52287095715006160, -23.47596703998600631, 11.44779298504228215 ) ) ;
#1792=CARTESIAN_POINT ( 'NONE',  ( -101.9195342205254775, -25.25419299847218468, 6.392810396799463390 ) ) ;
#1793=EDGE_CURVE ( 'NONE', #6687, #64842, #68245, .T. ) ;
#1794=B_SPLINE_CURVE_WITH_KNOTS ( 'NONE', 3,
 ( #82211, #21299, #66026, #13185 ),
 .UNSPECIFIED., .F., .F.,
 ( 4, 4 ),
 ( 0.000000000000000000, 9.999999999997510880E-05 ),
 .UNSPECIFIED. ) ;
#1795=CARTESIAN_POINT ( 'NONE',  ( -59.48968306854239074, -24.65952944569304961, 1.056160979905697905 ) ) ;
#1796=CARTESIAN_POINT ( 'NONE',  ( -109.3416230908480031, -25.31488395161200700, 5.187544736971523740 ) ) ;
#1797=CARTESIAN_POINT ( 'NONE',  ( -118.2228709571500787, -23.47596703998600631, 11.44779298504227860 ) ) ;
#1798=EDGE_CURVE ( 'NONE', #95755, #60161, #33850, .T. ) ;
#1799=CARTESIAN_POINT ( 'NONE',  ( -19.06252244145942498, 11.34236556261432405, 11.49999999999999645 ) ) ;
#1800=ORIENTED_EDGE ( 'NONE', *, *, #82331, .F. ) ;
#1802=CARTESIAN_POINT ( 'NONE',  ( -87.52287095715006160, -23.96127896942116564, -0.6493128930942591026 ) ) ;
#1804=CARTESIAN_POINT ( 'NONE',  ( 4.697487806458584991, -22.17256498326293013, -1.500000000000002220 ) ) ;
#1806=ORIENTED_EDGE ( 'NONE', *, *, #54260, .T. ) ;
#1807=ORIENTED_EDGE ( 'NONE', *, *, #90904, .F. ) ;
#1809=AXIS2_PLACEMENT_3D ( 'NONE', #23005, #15407, #46368 ) ;
#1811=CARTESIAN_POINT ( 'NONE',  ( 17.50376878386636292, -9.983289808088789741, -1.500000000000002220 ) ) ;
#1812=EDGE_CURVE ( 'NONE', #21561, #1208, #61144, .T. ) ;
#1813=CARTESIAN_POINT ( 'NONE',  ( -84.22287095715007865, -23.47596703998600276, 11.44779298504227683 ) ) ;
#1816=CARTESIAN_POINT ( 'NONE',  ( 10.13505985054399083, -19.98934331558005439, -1.500000000000002220 ) ) ;
#1818=EDGE_CURVE ( 'NONE', #79871, #5385, #1129, .T. ) ;
#1821=CARTESIAN_POINT ( 'NONE',  ( -112.6235203626142862, -24.66019654487200086, 8.947790411086112172 ) ) ;
#1822=CARTESIAN_POINT ( 'NONE',  ( -71.62287095715005592, -29.50248528299804818, 1.056150453629036701 ) ) ;
#1824=CARTESIAN_POINT ( 'NONE',  ( -41.52287095715006870, -24.51283580621450753, 0.6167428607045382094 ) ) ;
#1826=CARTESIAN_POINT ( 'NONE',  ( -63.94589839887400728, -23.78062553189672101, -0.9709657327914295033 ) ) ;
#1828=CARTESIAN_POINT ( 'NONE',  ( -1.979602623192304955, -19.45764201480039901, 11.49999999999998934 ) ) ;
#1830=ORIENTED_EDGE ( 'NONE', *, *, #16822, .F. ) ;
#1831=CARTESIAN_POINT ( 'NONE',  ( -5.607854029519995898, -20.77141283803394955, 11.49999999999998934 ) ) ;
#1832=CARTESIAN_POINT ( 'NONE',  ( -36.52287095715006870, -23.96127896941631263, -0.6493128931038070206 ) ) ;
#1834=DIRECTION ( 'NONE',  ( -3.773278334453079618E-23, 0.9999999999976377785, 2.173523156925978705E-06 ) ) ;
#1835=DIRECTION ( 'NONE',  ( 0.000000000000000000, -0.9999999999976377785, -2.173523156925979128E-06 ) ) ;
#1836=CARTESIAN_POINT ( 'NONE',  ( 21.44032754495887261, 8.191337786432022483, -1.500000000000002220 ) ) ;
#1837=B_SPLINE_CURVE_WITH_KNOTS ( 'NONE', 3,
 ( #8469, #93696, #857, #55662, #15571, #30806, #61275, #92196 ),
 .UNSPECIFIED., .F., .F.,
 ( 4, 2, 2, 4 ),
 ( -0.001224873891641422609, -0.0002244903592271080620, 0.0007758931731872060512, 0.002776660238015839048 ),
 .UNSPECIFIED. ) ;
#1840=CARTESIAN_POINT ( 'NONE',  ( -42.52287095715005449, -24.51283580621449687, 0.6167428607045715161 ) ) ;
#1841=CARTESIAN_POINT ( 'NONE',  ( -18.22994410263883225, 8.285605901428201747, 11.49999999999999645 ) ) ;
#1842=CARTESIAN_POINT ( 'NONE',  ( -78.96619831399281964, -25.31594569180612098, 5.670632933995499059 ) ) ;
#1843=CARTESIAN_POINT ( 'NONE',  ( -57.62287095715004881, -29.50250786944525672, 11.44777988621623876 ) ) ;
#1844=DIRECTION ( 'NONE',  ( 0.000000000000000000, 0.9999999999976377785, 2.173523156925979128E-06 ) ) ;
#1846=CARTESIAN_POINT ( 'NONE',  ( -72.62287095715005592, -24.65952944569304606, 1.056160979905698794 ) ) ;
#1847=CARTESIAN_POINT ( 'NONE',  ( -9.430186865587145917, -19.61854929170128869, -1.500000000000002220 ) ) ;
#1849=CARTESIAN_POINT ( 'NONE',  ( -8.122062702759739850, 17.86989387945112995, -1.500000000000002220 ) ) ;
#1850=FACE_OUTER_BOUND ( 'NONE', #89253, .T. ) ;
#1851=CARTESIAN_POINT ( 'NONE',  ( -41.62287095715007723, -24.35013146730203815, 9.818937971375117257 ) ) ;
#1852=CARTESIAN_POINT ( 'NONE',  ( -107.5228709571501042, -23.48783264083360578, -1.443836473376361118 ) ) ;
#1853=CARTESIAN_POINT ( 'NONE',  ( -67.52287095715006160, -29.50248528299804818, 1.056150453629036701 ) ) ;
#1854=CARTESIAN_POINT ( 'NONE',  ( 14.24201292913401140, 14.87178044790754328, 11.49999999999999645 ) ) ;
#1856=CARTESIAN_POINT ( 'NONE',  ( -120.5565315140265739, -23.85016227208581441, -0.8807180028928250914 ) ) ;
#1857=CARTESIAN_POINT ( 'NONE',  ( -19.94007547503736788, -10.58355046294204094, 11.49999999999999645 ) ) ;
#1858=EDGE_CURVE ( 'NONE', #24383, #30940, #20532, .T. ) ;
#1859=ORIENTED_EDGE ( 'NONE', *, *, #2198, .T. ) ;
#1860=CARTESIAN_POINT ( 'NONE',  ( -69.94684934828960365, -25.12219130708524517, 7.037048346111795638 ) ) ;
#1862=EDGE_CURVE ( 'NONE', #51996, #1269, #53030, .T. ) ;
#1864=CARTESIAN_POINT ( 'NONE',  ( -27.33104310173779083, -24.76554706090742997, 2.324039223911030572 ) ) ;
#1865=CARTESIAN_POINT ( 'NONE',  ( -33.62287095715005592, -24.64898659630367206, 1.056161002820817485 ) ) ;
#1867=ORIENTED_EDGE ( 'NONE', *, *, #39150, .F. ) ;
#1868=CARTESIAN_POINT ( 'NONE',  ( 8.651921485055520833, -21.43433228965458781, 11.49999999999999645 ) ) ;
#1869=CARTESIAN_POINT ( 'NONE',  ( -16.39533425382319720, 15.89506036719111037, 11.49999999999998934 ) ) ;
#1871=PLANE ( 'NONE',  #62529 ) ;
#1872=CARTESIAN_POINT ( 'NONE',  ( -63.51555983570501951, -23.73791477778911840, 11.05961554403170766 ) ) ;
#1873=CARTESIAN_POINT ( 'NONE',  ( 8.413247042826936806, 20.86129769029627923, 11.49999999999999645 ) ) ;
#1876=VECTOR ( 'NONE', #78946, 1000.000000000000227 ) ;
#1877=CARTESIAN_POINT ( 'NONE',  ( -6.887433846447126307, -20.85920400149894149, 11.49999999999998934 ) ) ;
#1878=CARTESIAN_POINT ( 'NONE',  ( -124.5120803120196058, -25.40057329153380650, 4.607783471004946563 ) ) ;
#1879=EDGE_CURVE ( 'NONE', #45924, #50012, #83431, .T. ) ;
#1880=DIRECTION ( 'NONE',  ( -3.773278334453079618E-23, 0.9999999999976377785, 2.173523156925979975E-06 ) ) ;
#1882=ORIENTED_EDGE ( 'NONE', *, *, #49450, .F. ) ;
#1884=FACE_OUTER_BOUND ( 'NONE', #6110, .T. ) ;
#1886=B_SPLINE_CURVE_WITH_KNOTS ( 'NONE', 3,
 ( #69587, #16788, #46242, #9683, #85807, #7678, #40642, #55876, #93910, #31512, #24401, #63494, #62475, #47754, #16287, #78174, #79187, #78668 ),
 .UNSPECIFIED., .F., .F.,
 ( 4, 2, 2, 2, 2, 2, 2, 2, 4 ),
 ( 1.411962612463446054E-17, 0.0002845812759709316587, 0.0005691625519418492228, 0.0008537438279127667869, 0.001138325103883684351, 0.001422906379854601807, 0.001707487655825519479, 0.001992068931796437369, 0.002276650207767354824 ),
 .UNSPECIFIED. ) ;
#1887=CARTESIAN_POINT ( 'NONE',  ( -19.82921842031888104, 5.099586017421429140, -1.500000000000002220 ) ) ;
#1888=VERTEX_POINT ( 'NONE', #28682 ) ;
#1889=EDGE_CURVE ( 'NONE', #42461, #81255, #61718, .T. ) ;
#1892=ORIENTED_EDGE ( 'NONE', *, *, #6915, .T. ) ;
#1893=CARTESIAN_POINT ( 'NONE',  ( 17.26854690438276307, -15.35948741044508559, 11.49999999999998934 ) ) ;
#1894=LINE ( 'NONE', #93724, #94085 ) ;
#1895=CARTESIAN_POINT ( 'NONE',  ( 19.83649001621966335, 4.521578618930774951, -1.500000000000002220 ) ) ;
#1898=DIRECTION ( 'NONE',  ( -3.773278334444167608E-23, 1.000000000000000000, 0.000000000000000000 ) ) ;
#1899=ADVANCED_FACE ( 'NONE', ( #77330 ), #8836, .T. ) ;
#1901=EDGE_CURVE ( 'NONE', #75398, #88641, #47404, .T. ) ;
#1903=CARTESIAN_POINT ( 'NONE',  ( -39.92287095715006018, -23.47596703998600276, 11.44779298504227683 ) ) ;
#1905=CARTESIAN_POINT ( 'NONE',  ( 3.930203739357332360, 21.12693704021120666, 11.49999999999999645 ) ) ;
#1907=CARTESIAN_POINT ( 'NONE',  ( -75.52207693552151113, -23.48783264082477018, -1.443836473390089914 ) ) ;
#1908=CARTESIAN_POINT ( 'NONE',  ( -48.52287095715006160, -24.64898659630367561, 1.056161002820821038 ) ) ;
#1912=CARTESIAN_POINT ( 'NONE',  ( 8.056674255711671506, 19.11000797562349618, -1.500000000000002220 ) ) ;
#1913=VERTEX_POINT ( 'NONE', #70740 ) ;
#1914=CARTESIAN_POINT ( 'NONE',  ( -57.52287095715005449, -23.48786465467241058, 11.44779295918254824 ) ) ;
#1915=VERTEX_POINT ( 'NONE', #23537 ) ;
#1918=EDGE_LOOP ( 'NONE', ( #48605, #100308, #46695, #93169 ) ) ;
#1919=ORIENTED_EDGE ( 'NONE', *, *, #78108, .F. ) ;
#1921=CARTESIAN_POINT ( 'NONE',  ( -42.60032671284469785, -23.96169478059713143, 10.65365249895718947 ) ) ;
#1922=CARTESIAN_POINT ( 'NONE',  ( -29.58730922106722261, -25.09253774316045238, 3.113369324251616277 ) ) ;
#1923=EDGE_CURVE ( 'NONE', #53590, #63195, #70237, .T. ) ;
#1924=EDGE_CURVE ( 'NONE', #24545, #91623, #5979, .T. ) ;
#1925=CARTESIAN_POINT ( 'NONE',  ( 20.91424602935089894, 6.983905699820807556, 11.49999999999999645 ) ) ;
#1928=CARTESIAN_POINT ( 'NONE',  ( -21.70561270324154179, 6.225854807558039994, 11.49999999999998934 ) ) ;
#1929=CARTESIAN_POINT ( 'NONE',  ( 19.54352652498339182, 7.673529024697476331, 11.49999999999998934 ) ) ;
#1938=ORIENTED_EDGE ( 'NONE', *, *, #59876, .F. ) ;
#1939=CARTESIAN_POINT ( 'NONE',  ( 1.363997202867437863, 21.09336101032836908, 11.49999999999998934 ) ) ;
#1940=CARTESIAN_POINT ( 'NONE',  ( -117.5562042904833930, -23.47593901973091235, -1.443836447538997536 ) ) ;
#1941=CARTESIAN_POINT ( 'NONE',  ( -60.72703938549737046, -25.27183489919806192, 3.712349809207165841 ) ) ;
#1942=CARTESIAN_POINT ( 'NONE',  ( -75.62287095715012697, -24.51163499207175533, 0.6490370598554298098 ) ) ;
#1945=CARTESIAN_POINT ( 'NONE',  ( 21.95989154999629278, -3.605859658025859282, -1.500000000000002220 ) ) ;
#1946=CARTESIAN_POINT ( 'NONE',  ( -114.5206660350143721, -23.73766607897672287, -1.055555164236428700 ) ) ;
#1947=ADVANCED_FACE ( 'NONE', ( #24049 ), #78826, .T. ) ;
#1950=CARTESIAN_POINT ( 'NONE',  ( -58.58953762381673869, -23.47596703998600276, 11.44779298504227505 ) ) ;
#1952=EDGE_CURVE ( 'NONE', #32503, #21619, #46399, .T. ) ;
#1954=CARTESIAN_POINT ( 'NONE',  ( -33.62287095715005592, -24.50321055353805377, 9.387540953477536476 ) ) ;
#1955=EDGE_CURVE ( 'NONE', #57577, #79844, #92562, .T. ) ;
#1956=CARTESIAN_POINT ( 'NONE',  ( -7.007757480239389380, 18.17491015770016816, -1.500000000000002220 ) ) ;
#1957=CARTESIAN_POINT ( 'NONE',  ( -5.333777546869826303, -20.73983961313815172, -1.500000000000002220 ) ) ;
#1958=FACE_OUTER_BOUND ( 'NONE', #29896, .T. ) ;
#1959=CARTESIAN_POINT ( 'NONE',  ( -60.48802560456093147, -24.73531770709804078, 8.716586749031112191 ) ) ;
#1960=VECTOR ( 'NONE', #62384, 1000.000000000000114 ) ;
#1961=CARTESIAN_POINT ( 'NONE',  ( -51.56792531176364491, -23.48783264082476308, -1.443836473390094133 ) ) ;
#1962=CARTESIAN_POINT ( 'NONE',  ( -52.52287095715008292, -24.66019654487198665, 8.947790411086131712 ) ) ;
#1963=CARTESIAN_POINT ( 'NONE',  ( 15.01325480956343483, 17.08929600257393489, -1.500000000000002220 ) ) ;
#1965=FACE_OUTER_BOUND ( 'NONE', #63215, .T. ) ;
#1967=CARTESIAN_POINT ( 'NONE',  ( 7.713363164125232707, -18.29545692620113684, 11.49999999999999645 ) ) ;
#1968=CARTESIAN_POINT ( 'NONE',  ( -123.5190355150976416, -24.66019654487200441, 8.947790411086106843 ) ) ;
#1969=CARTESIAN_POINT ( 'NONE',  ( -108.5562042904834072, -23.48786465467241769, 11.44779295918254292 ) ) ;
#1970=CARTESIAN_POINT ( 'NONE',  ( -64.92287095715006728, -23.47593901973090169, -1.443836447538997536 ) ) ;
#1973=CARTESIAN_POINT ( 'NONE',  ( -80.52287095715009002, -24.62285846331441874, 9.038163153548151030 ) ) ;
#1974=CARTESIAN_POINT ( 'NONE',  ( -51.52876458270549165, -25.27412355576682046, 3.420678484884101422 ) ) ;
#1975=CARTESIAN_POINT ( 'NONE',  ( -2.129050106866105185, 21.58297100922832357, -1.500000000000002220 ) ) ;
#1976=CARTESIAN_POINT ( 'NONE',  ( -56.63815877224512718, -24.15620529776628445, 10.23563542870660648 ) ) ;
#1977=CARTESIAN_POINT ( 'NONE',  ( 1.255614643274026276, -19.41590359075080841, -1.500000000000002220 ) ) ;
#1978=DIRECTION ( 'NONE',  ( 0.000000000000000000, 0.9999999999976377785, 2.173523156925979128E-06 ) ) ;
#1982=CARTESIAN_POINT ( 'NONE',  ( 9.511415417357532931, -18.05363124325620205, 11.49999999999999645 ) ) ;
#1983=DIRECTION ( 'NONE',  ( -3.773278334444167608E-23, 1.000000000000000000, 0.000000000000000000 ) ) ;
#1985=ORIENTED_EDGE ( 'NONE', *, *, #91939, .F. ) ;
#1986=CARTESIAN_POINT ( 'NONE',  ( -79.70293883480100305, -25.07319016999186090, 7.368904005479246955 ) ) ;
#1989=CARTESIAN_POINT ( 'NONE',  ( -49.35642674012009223, -25.25138802042284780, 5.792946750273627821 ) ) ;
#1991=CARTESIAN_POINT ( 'NONE',  ( -109.6330755333671334, -23.48783264082476663, -1.443836473390089470 ) ) ;
#1992=ORIENTED_EDGE ( 'NONE', *, *, #54926, .F. ) ;
#1993=CARTESIAN_POINT ( 'NONE',  ( -66.54416241931652110, -24.35071581493543036, 9.817618358456028815 ) ) ;
#1994=CARTESIAN_POINT ( 'NONE',  ( -22.40196285382242536, -4.882868457752029379, 11.49999999999999645 ) ) ;
#1995=CARTESIAN_POINT ( 'NONE',  ( 2.440706796964721370, 22.61111150098722788, 11.49999999999998934 ) ) ;
#1996=ORIENTED_EDGE ( 'NONE', *, *, #78456, .T. ) ;
#1997=CARTESIAN_POINT ( 'NONE',  ( -81.42380231474228935, -25.31401921878147832, 5.197788989978542773 ) ) ;
#1998=CARTESIAN_POINT ( 'NONE',  ( -98.52287095715000476, -23.96127896941632329, -0.6493128931038036900 ) ) ;
#1999=CARTESIAN_POINT ( 'NONE',  ( -123.6228709571500559, -24.66019654487200086, 8.947790411086117501 ) ) ;
#2000=FACE_OUTER_BOUND ( 'NONE', #25505, .T. ) ;
#2001=B_SPLINE_CURVE_WITH_KNOTS ( 'NONE', 3,
 ( #20370, #51344, #57973, #34125, #88912, #50350 ),
 .UNSPECIFIED., .F., .F.,
 ( 4, 2, 4 ),
 ( 6.391158118959990520E-06, 0.001387004593080774003, 0.002767618028042588118 ),
 .UNSPECIFIED. ) ;
#2002=CARTESIAN_POINT ( 'NONE',  ( -69.55927315202205818, -23.73791477778911485, 11.05961554403170766 ) ) ;
#2004=ADVANCED_FACE ( 'NONE', ( #2239 ), #61642, .T. ) ;
#2007=CARTESIAN_POINT ( 'NONE',  ( -58.59839962558949367, -23.96119346886880308, -0.6495511937832116889 ) ) ;
#2008=ORIENTED_EDGE ( 'NONE', *, *, #79429, .T. ) ;
#2010=CARTESIAN_POINT ( 'NONE',  ( 7.100489274569507181, 19.11111018586187527, -1.500000000000002220 ) ) ;
#2011=ORIENTED_EDGE ( 'NONE', *, *, #39501, .T. ) ;
#2013=ORIENTED_EDGE ( 'NONE', *, *, #40219, .T. ) ;
#2014=B_SPLINE_CURVE_WITH_KNOTS ( 'NONE', 3,
 ( #18320, #31531, #70602, #1094, #50778, #81719, #42675, #96441, #57406, #12191, #65027, #3114, #81219, #35050, #27438, #74595 ),
 .UNSPECIFIED., .F., .F.,
 ( 4, 2, 2, 2, 2, 2, 2, 4 ),
 ( 1.939467588463157335E-15, 0.0001875988099759247666, 0.0003751976199499100582, 0.0007503952398979218952, 0.001125592859845933732, 0.001313191669819952770, 0.001406991074806955566, 0.001500790479793958363 ),
 .UNSPECIFIED. ) ;
#2015=CARTESIAN_POINT ( 'NONE',  ( 17.37538969058663696, -15.08583811485692117, -1.500000000000002220 ) ) ;
#2016=CARTESIAN_POINT ( 'NONE',  ( -117.5228709571500758, -29.50250243563736774, 8.947779886222134493 ) ) ;
#2020=EDGE_CURVE ( 'NONE', #58811, #25123, #52001, .T. ) ;
#2023=CARTESIAN_POINT ( 'NONE',  ( -95.63508492949864603, -24.15503026093913874, -0.2815557561904519224 ) ) ;
#2024=CARTESIAN_POINT ( 'NONE',  ( -116.7734655731286182, -25.27149756095137434, 5.922859442452534928 ) ) ;
#2025=CARTESIAN_POINT ( 'NONE',  ( 17.78463046036513617, -11.72987588014745342, 11.49999999999999645 ) ) ;
#2027=VECTOR ( 'NONE', #28920, 1000.000000000000114 ) ;
#2028=EDGE_CURVE ( 'NONE', #40347, #89809, #11829, .T. ) ;
#2029=ORIENTED_EDGE ( 'NONE', *, *, #23760, .F. ) ;
#2030=CARTESIAN_POINT ( 'NONE',  ( -15.91109736606077441, 15.52988587838853540, -1.500000000000002220 ) ) ;
#2031=VECTOR ( 'NONE', #33172, 1000.000000000000114 ) ;
#2032=CARTESIAN_POINT ( 'NONE',  ( 10.45329875151443488, -17.81600612866554556, -1.500000000000002220 ) ) ;
#2033=EDGE_LOOP ( 'NONE', ( #7120, #78790, #20221, #31481 ) ) ;
#2035=CARTESIAN_POINT ( 'NONE',  ( -95.50800993025161745, -24.52399227489127398, 9.353111116836524630 ) ) ;
#2036=ORIENTED_EDGE ( 'NONE', *, *, #31919, .T. ) ;
#2038=ORIENTED_EDGE ( 'NONE', *, *, #68252, .T. ) ;
#2039=CARTESIAN_POINT ( 'NONE',  ( -58.57884717839115751, -24.66019654487199730, 8.947790411086117501 ) ) ;
#2041=CARTESIAN_POINT ( 'NONE',  ( 7.204507412156021751, -19.57454612608841771, -1.500000000000002220 ) ) ;
#2043=CARTESIAN_POINT ( 'NONE',  ( -21.44618410820073606, 4.064364382921047181, 11.49999999999999645 ) ) ;
#2044=CARTESIAN_POINT ( 'NONE',  ( -73.49932069601484841, -24.51419770103157347, 9.386484678747175181 ) ) ;
#2046=CARTESIAN_POINT ( 'NONE',  ( 22.08653571170524543, -4.319401766784854324, -1.500000000000002220 ) ) ;
#2047=CARTESIAN_POINT ( 'NONE',  ( -50.41800648699645393, -25.31296764934565857, 4.735575929649717963 ) ) ;
#2049=VECTOR ( 'NONE', #70329, 1000.000000000000114 ) ;
#2050=CARTESIAN_POINT ( 'NONE',  ( -54.58953762381672448, -24.65952944569304606, 1.056160979905695463 ) ) ;
#2054=ORIENTED_EDGE ( 'NONE', *, *, #72940, .T. ) ;
#2056=CARTESIAN_POINT ( 'NONE',  ( -99.31542661674430406, -25.26221151531081333, 6.334584452247769448 ) ) ;
#2058=CARTESIAN_POINT ( 'NONE',  ( -9.924231251898440576, -18.97836718215353713, -1.500000000000002220 ) ) ;
#2060=CARTESIAN_POINT ( 'NONE',  ( -21.16225983376422448, 7.283793490815352989, 11.49999999999999645 ) ) ;
#2063=CARTESIAN_POINT ( 'NONE',  ( -13.06023916655064276, -16.53025015627232719, 11.49999999999998934 ) ) ;
#2064=CARTESIAN_POINT ( 'NONE',  ( -30.46620467572866886, -25.14197234194089603, 7.291421475381016926 ) ) ;
#2065=CARTESIAN_POINT ( 'NONE',  ( -14.97016004668225264, 13.15154794113874637, -1.500000000000002220 ) ) ;
#2066=CARTESIAN_POINT ( 'NONE',  ( -50.58239890853555210, -24.73531770709094602, 8.716586749053508498 ) ) ;
#2067=CARTESIAN_POINT ( 'NONE',  ( -80.74930246458728789, -25.30877083504385183, 4.554285748811262025 ) ) ;
#2068=CARTESIAN_POINT ( 'NONE',  ( 22.04941498731238525, 0.3350016526185666255, -1.500000000000002220 ) ) ;
#2069=AXIS2_PLACEMENT_3D ( 'NONE', #60460, #20864, #13748 ) ;
#2070=ORIENTED_EDGE ( 'NONE', *, *, #93615, .T. ) ;
#2071=CARTESIAN_POINT ( 'NONE',  ( -111.5228709571500616, -29.50248528299804818, 1.056150453629043584 ) ) ;
#2072=LINE ( 'NONE', #73081, #78951 ) ;
#2073=CARTESIAN_POINT ( 'NONE',  ( -20.60679684081203789, -3.318877370925724879, 11.49999999999999645 ) ) ;
#2074=EDGE_CURVE ( 'NONE', #46475, #7077, #22846, .T. ) ;
#2077=CARTESIAN_POINT ( 'NONE',  ( -63.52287095715003318, -23.48783264082477018, -1.443836473390091690 ) ) ;
#2078=CARTESIAN_POINT ( 'NONE',  ( -16.05942832139214360, -14.02155611864158402, 11.49999999999998934 ) ) ;
#2079=CARTESIAN_POINT ( 'NONE',  ( -121.6228709571500417, -24.64965695001469115, 8.947790433994175174 ) ) ;
#2080=CARTESIAN_POINT ( 'NONE',  ( -124.5228709571500616, -24.64898659630368627, 1.056161002820833028 ) ) ;
#2082=CARTESIAN_POINT ( 'NONE',  ( -71.52287095715007581, -24.65952944569304606, 1.056160979905697239 ) ) ;
#2084=CARTESIAN_POINT ( 'NONE',  ( 22.24477432615492134, 4.004077059304647968, -1.500000000000002220 ) ) ;
#2086=B_SPLINE_SURFACE_WITH_KNOTS ( 'NONE', 3, 3, ( 
 ( #86519, #88033, #79906, #48478 ),
 ( #78895, #72308, #17005, #64723 ),
 ( #64213, #18507, #47970, #9393 ),
 ( #86021, #10396, #56088, #39347 ),
 ( #70306, #40354, #1297, #17511 ),
 ( #95640, #71308, #71812, #79404 ),
 ( #31738, #62706, #93621, #1795 ) ),
 .UNSPECIFIED., .F., .F., .F.,
 ( 4, 3, 4 ),
 ( 4, 4 ),
 ( 0.0004766839783814567867, 0.1029713700210892341, 0.2054660560637970035 ),
 ( 0.7096745263232591139, 0.7110146934017589349 ),
 .UNSPECIFIED. ) ;
#2087=CARTESIAN_POINT ( 'NONE',  ( -83.52287095715001897, -24.66019654487199375, 8.947790411086122830 ) ) ;
#2088=ORIENTED_EDGE ( 'NONE', *, *, #16133, .F. ) ;
#2090=CARTESIAN_POINT ( 'NONE',  ( -122.6228709571500417, -23.72747288104442021, -1.053458166803660667 ) ) ;
#2091=CARTESIAN_POINT ( 'NONE',  ( -3.719764837209879271, -19.30396570740023421, 11.49999999999999645 ) ) ;
#2093=B_SPLINE_CURVE_WITH_KNOTS ( 'NONE', 3,
 ( #83373, #29589, #14357, #29091 ),
 .UNSPECIFIED., .F., .F.,
 ( 4, 4 ),
 ( 0.000000000000000000, 9.999999999998897304E-05 ),
 .UNSPECIFIED. ) ;
#2094=B_SPLINE_CURVE_WITH_KNOTS ( 'NONE', 3,
 ( #35128, #89408, #80801, #73193 ),
 .UNSPECIFIED., .F., .F.,
 ( 4, 4 ),
 ( 2.775557561562891351E-17, 0.0001000000000000167286 ),
 .UNSPECIFIED. ) ;
#2097=CARTESIAN_POINT ( 'NONE',  ( -99.55261637441094535, -24.15543982623907837, -0.2315651400026449425 ) ) ;
#2098=LINE ( 'NONE', #48263, #99884 ) ;
#2102=PLANE ( 'NONE',  #22159 ) ;
#2103=CARTESIAN_POINT ( 'NONE',  ( 17.76913753361954562, 8.601950719843506121, 11.49999999999998934 ) ) ;
#2104=ORIENTED_EDGE ( 'NONE', *, *, #39676, .F. ) ;
#2105=AXIS2_PLACEMENT_3D ( 'NONE', #47774, #55896, #84814 ) ;
#2106=CARTESIAN_POINT ( 'NONE',  ( -17.27845874757997535, -10.49745931960568335, 11.49999999999999645 ) ) ;
#2109=DIRECTION ( 'NONE',  ( 0.000000000000000000, 0.9999999999976377785, 2.173523156925979128E-06 ) ) ;
#2110=CARTESIAN_POINT ( 'NONE',  ( -80.43221577628075636, -25.30553498687082481, 4.967019777649441359 ) ) ;
#2111=CARTESIAN_POINT ( 'NONE',  ( -100.2380303841250395, -25.03145177541831856, 7.557071270405856467 ) ) ;
#2112=CARTESIAN_POINT ( 'NONE',  ( -82.62287095715002749, -24.33832256527049154, 0.1851278514138593179 ) ) ;
#2114=CARTESIAN_POINT ( 'NONE',  ( -120.6228709571500559, -23.48786465467241769, 11.44779295918253759 ) ) ;
#2115=CARTESIAN_POINT ( 'NONE',  ( 16.76344175524385705, -10.90933549886441156, -1.500000000000002220 ) ) ;
#2116=CARTESIAN_POINT ( 'NONE',  ( -99.21726371882367346, -25.10935196860294383, 3.564825239790214706 ) ) ;
#2117=FACE_OUTER_BOUND ( 'NONE', #39200, .T. ) ;
#2122=CARTESIAN_POINT ( 'NONE',  ( -78.62287095715007013, -24.66019654487199375, 8.947790411086124607 ) ) ;
#2123=CARTESIAN_POINT ( 'NONE',  ( -92.62287095715005592, -23.47596703998600631, 11.44779298504227860 ) ) ;
#2124=B_SPLINE_CURVE_WITH_KNOTS ( 'NONE', 3,
 ( #69059, #546, #93896, #53350 ),
 .UNSPECIFIED., .F., .F.,
 ( 4, 4 ),
 ( 0.000000000000000000, 1.000000000000000000 ),
 .UNSPECIFIED. ) ;
#2125=CARTESIAN_POINT ( 'NONE',  ( -116.5120803120195916, -25.40057329153378518, 4.607783471004933240 ) ) ;
#2126=CARTESIAN_POINT ( 'NONE',  ( -51.69903695958453227, -25.26279909962675774, 4.034228678170331150 ) ) ;
#2127=CARTESIAN_POINT ( 'NONE',  ( -63.62287095715007723, -24.35013146730203459, 9.818937971375108376 ) ) ;
#2129=ADVANCED_FACE ( 'NONE', ( #41290 ), #84634, .T. ) ;
#2132=EDGE_CURVE ( 'NONE', #23327, #77908, #32568, .T. ) ;
#2133=CARTESIAN_POINT ( 'NONE',  ( 18.82434097252966154, -7.598309640217090433, 11.49999999999998934 ) ) ;
#2136=ADVANCED_FACE ( 'NONE', ( #68618 ), #35678, .T. ) ;
#2137=CARTESIAN_POINT ( 'NONE',  ( -114.6228709571500417, -23.94994826722566117, -0.6494450866342732498 ) ) ;
#2138=CARTESIAN_POINT ( 'NONE',  ( -59.58753039450819955, -24.35071581493543746, 9.817618358456035921 ) ) ;
#2139=ADVANCED_FACE ( 'NONE', ( #51401 ), #92739, .T. ) ;
#2140=VERTEX_POINT ( 'NONE', #45779 ) ;
#2143=CARTESIAN_POINT ( 'NONE',  ( -7.596101150008887082, -19.70107428960382734, 11.49999999999999645 ) ) ;
#2144=CARTESIAN_POINT ( 'NONE',  ( 13.35222405703702186, 17.66689192352044913, -1.500000000000002220 ) ) ;
#2145=EDGE_CURVE ( 'NONE', #18949, #85237, #56873, .T. ) ;
#2146=CARTESIAN_POINT ( 'NONE',  ( -14.18348626307465743, -14.89297910716571849, 11.49999999999998934 ) ) ;
#2148=CARTESIAN_POINT ( 'NONE',  ( -66.52287095715006160, -23.47596703998600631, 11.44779298504228748 ) ) ;
#2150=CARTESIAN_POINT ( 'NONE',  ( -54.50804670033233634, -23.96119346886879953, -0.6495511937832153526 ) ) ;
#2151=CARTESIAN_POINT ( 'NONE',  ( -85.62287095715005592, -23.47593901973091235, -1.443836447539002865 ) ) ;
#2152=ORIENTED_EDGE ( 'NONE', *, *, #37751, .F. ) ;
#2153=ORIENTED_EDGE ( 'NONE', *, *, #85977, .F. ) ;
#2155=CARTESIAN_POINT ( 'NONE',  ( -100.5228709571500758, -24.14321612903116687, -0.2833117244521499156 ) ) ;
#2156=LINE ( 'NONE', #54931, #58393 ) ;
#2157=CARTESIAN_POINT ( 'NONE',  ( -91.62287095715004170, -23.48783264082478794, -1.443836473390063713 ) ) ;
#2158=CARTESIAN_POINT ( 'NONE',  ( 20.67342648114324533, -1.018679444107209342, -1.500000000000002220 ) ) ;
#2159=CARTESIAN_POINT ( 'NONE',  ( -2.787017431591729988, -21.48445716988565835, 11.49999999999999645 ) ) ;
#2160=ORIENTED_EDGE ( 'NONE', *, *, #9653, .T. ) ;
#2162=CARTESIAN_POINT ( 'NONE',  ( -60.52287095715005449, -24.15516710230758690, 10.28746687062794152 ) ) ;
#2164=CARTESIAN_POINT ( 'NONE',  ( 11.64234319522276095, -19.14997049866658330, 11.49999999999998934 ) ) ;
#2165=PLANE ( 'NONE',  #86966 ) ;
#2166=CARTESIAN_POINT ( 'NONE',  ( -71.62287095715005592, -23.48786465467241413, 11.44779295918254469 ) ) ;
#2167=ORIENTED_EDGE ( 'NONE', *, *, #54005, .F. ) ;
#2169=CARTESIAN_POINT ( 'NONE',  ( -120.6228709571500559, -23.48786465467241769, 11.44779295918253759 ) ) ;
#2170=VECTOR ( 'NONE', #99538, 1000.000000000000114 ) ;
#2171=EDGE_LOOP ( 'NONE', ( #66024, #70525, #40165, #28479 ) ) ;
#2172=ORIENTED_EDGE ( 'NONE', *, *, #30820, .F. ) ;
#2174=ORIENTED_EDGE ( 'NONE', *, *, #58731, .F. ) ;
#2176=B_SPLINE_CURVE_WITH_KNOTS ( 'NONE', 3,
 ( #24067, #94080, #6851, #47420, #14955, #62656, #61657, #93077, #31180, #14455, #32181, #39296, #15455, #92083, #78348, #46917 ),
 .UNSPECIFIED., .F., .F.,
 ( 4, 2, 2, 2, 2, 2, 2, 4 ),
 ( 0.000000000000000000, 0.0002756755153052838146, 0.0005513510306105676292, 0.001102702061221115526, 0.001378377576526390071, 0.001654053091831664615, 0.001929728607136938943, 0.002205404122442214572 ),
 .UNSPECIFIED. ) ;
#2177=CARTESIAN_POINT ( 'NONE',  ( 20.85495618715548716, -4.085033163991189653, -1.500000000000002220 ) ) ;
#2178=ORIENTED_EDGE ( 'NONE', *, *, #51492, .T. ) ;
#2179=FACE_OUTER_BOUND ( 'NONE', #39740, .T. ) ;
#2180=CARTESIAN_POINT ( 'NONE',  ( -21.66901994843296819, -2.608494568651300138, -1.500000000000002220 ) ) ;
#2181=CARTESIAN_POINT ( 'NONE',  ( -52.54157490255303742, -24.35071581493542681, 9.817618358456037697 ) ) ;
#2184=CARTESIAN_POINT ( 'NONE',  ( 8.256513476402210117, 20.27555108428041208, -1.500000000000002220 ) ) ;
#2185=CARTESIAN_POINT ( 'NONE',  ( -30.57287095715006231, -23.47596702059239604, 11.43887032355635647 ) ) ;
#2186=ORIENTED_EDGE ( 'NONE', *, *, #84467, .F. ) ;
#2188=CARTESIAN_POINT ( 'NONE',  ( -48.87479414115020404, -25.26337311648806505, 6.180417640909889876 ) ) ;
#2190=ORIENTED_EDGE ( 'NONE', *, *, #25403, .T. ) ;
#2192=EDGE_LOOP ( 'NONE', ( #92417, #42503, #1396, #21494 ) ) ;
#2193=CARTESIAN_POINT ( 'NONE',  ( -58.55620429048339304, -24.64965694238575011, 8.947790433994200043 ) ) ;
#2194=CARTESIAN_POINT ( 'NONE',  ( -31.24388727629347784, -25.31586941165988236, 4.461292436448222709 ) ) ;
#2195=CARTESIAN_POINT ( 'NONE',  ( 10.86157628581156764, 18.25448884030880592, -1.500000000000002220 ) ) ;
#2197=CARTESIAN_POINT ( 'NONE',  ( -30.59367615247571592, -24.87212640336024805, 1.420893871182736579 ) ) ;
#2198=EDGE_CURVE ( 'NONE', #34988, #6691, #85775, .T. ) ;
#2199=PLANE ( 'NONE',  #51884 ) ;
#2200=CARTESIAN_POINT ( 'NONE',  ( -48.62287095715004881, -23.47596703998600276, 11.44779298504227505 ) ) ;
#2201=VECTOR ( 'NONE', #51397, 1000.000000000000114 ) ;
#2202=CARTESIAN_POINT ( 'NONE',  ( 7.305494252837257285, 17.95555029072639286, -1.500000000000002220 ) ) ;
#2203=EDGE_CURVE ( 'NONE', #44804, #28633, #87035, .T. ) ;
#2204=CARTESIAN_POINT ( 'NONE',  ( -45.59298552244553093, -24.40034930558990922, 0.3402023900116019073 ) ) ;
#2206=CARTESIAN_POINT ( 'NONE',  ( -19.34354882100874562, 2.624169249526263403, 11.49999999999999645 ) ) ;
#2208=VECTOR ( 'NONE', #77039, 1000.000000000000114 ) ;
#2210=ORIENTED_EDGE ( 'NONE', *, *, #62270, .T. ) ;
#2212=CARTESIAN_POINT ( 'NONE',  ( -119.5562042904833788, -24.64965694238574656, 8.947790433994191162 ) ) ;
#2213=CARTESIAN_POINT ( 'NONE',  ( -90.52287095715013265, -24.83602698348160231, 1.605859176311266179 ) ) ;
#2214=CARTESIAN_POINT ( 'NONE',  ( -81.60636161561390622, -25.03155942975127246, 7.020725065118214481 ) ) ;
#2215=CARTESIAN_POINT ( 'NONE',  ( 10.71975780190685690, -16.47196428025586812, 11.49999999999998934 ) ) ;
#2216=ORIENTED_EDGE ( 'NONE', *, *, #83961, .T. ) ;
#2218=DIRECTION ( 'NONE',  ( 0.000000000000000000, -0.9999999999976377785, -2.173523156925979128E-06 ) ) ;
#2222=CARTESIAN_POINT ( 'NONE',  ( -33.52287095715006160, -29.50250243563736774, 8.947779886222150481 ) ) ;
#2223=CARTESIAN_POINT ( 'NONE',  ( -105.5562042904834072, -23.48786465467241769, 11.44779295918254292 ) ) ;
#2224=CARTESIAN_POINT ( 'NONE',  ( -50.40445135320379677, -29.50249014687182836, 3.293933732389337621 ) ) ;
#2225=FACE_OUTER_BOUND ( 'NONE', #97700, .T. ) ;
#2226=CARTESIAN_POINT ( 'NONE',  ( -43.62287095715004881, -24.66019654487199020, 8.947790411086135265 ) ) ;
#2227=CARTESIAN_POINT ( 'NONE',  ( -69.34512923434627396, -25.31201765456443198, 6.118189256283883104 ) ) ;
#2229=CARTESIAN_POINT ( 'NONE',  ( -11.57717615966994273, 16.22069937712612031, -1.500000000000002220 ) ) ;
#2231=CARTESIAN_POINT ( 'NONE',  ( -100.8449020736807711, -25.20544635972949266, 3.368783707514380499 ) ) ;
#2232=CARTESIAN_POINT ( 'NONE',  ( 6.283368587668265448, -18.83516890145298106, -1.500000000000002220 ) ) ;
#2234=CARTESIAN_POINT ( 'NONE',  ( -115.5228709571500616, -25.00158670708909625, 2.256160236439166411 ) ) ;
#2238=CARTESIAN_POINT ( 'NONE',  ( -7.357705842588929457, 19.43699106120834230, 11.49999999999999645 ) ) ;
#2239=FACE_OUTER_BOUND ( 'NONE', #63813, .T. ) ;
#2240=DIRECTION ( 'NONE',  ( 1.000000000000000000, 3.773278334444167608E-23, 8.201307833595939069E-29 ) ) ;
#2241=CARTESIAN_POINT ( 'NONE',  ( 22.67573665902413182, 1.879276792517311501, 11.49999999999999645 ) ) ;
#2243=CARTESIAN_POINT ( 'NONE',  ( -91.62287095715004170, -24.50216790748205753, 0.6166512839542586111 ) ) ;
#2244=LINE ( 'NONE', #34189, #71142 ) ;
#2245=ORIENTED_EDGE ( 'NONE', *, *, #13130, .F. ) ;
#2246=CARTESIAN_POINT ( 'NONE',  ( -14.42758394406654610, -14.16023863206117994, -1.500000000000002220 ) ) ;
#2248=CARTESIAN_POINT ( 'NONE',  ( -69.52287095715009002, -23.48783264082477018, -1.443836473390092801 ) ) ;
#2250=EDGE_CURVE ( 'NONE', #59253, #19418, #50745, .T. ) ;
#2251=ORIENTED_EDGE ( 'NONE', *, *, #35979, .F. ) ;
#2253=CARTESIAN_POINT ( 'NONE',  ( -51.62287095715004881, -24.51283580621364067, 0.6167428607019803666 ) ) ;
#2254=CARTESIAN_POINT ( 'NONE',  ( -20.00956492049148494, -0.6725752471728385640, -1.500000000000002220 ) ) ;
#2256=EDGE_CURVE ( 'NONE', #51872, #38706, #25398, .T. ) ;
#2257=CARTESIAN_POINT ( 'NONE',  ( -19.40599490818632233, 7.965113791304038848, 11.49999999999999645 ) ) ;
#2260=CARTESIAN_POINT ( 'NONE',  ( 10.81757466760856801, -19.22619917341675588, 11.49999999999998934 ) ) ;
#2261=EDGE_CURVE ( 'NONE', #71061, #44804, #55604, .T. ) ;
#2262=CARTESIAN_POINT ( 'NONE',  ( -127.4728709548940486, -25.40673988423724339, 2.000950539785686821 ) ) ;
#2264=VERTEX_POINT ( 'NONE', #77707 ) ;
#2265=CARTESIAN_POINT ( 'NONE',  ( -36.62287095715005592, -29.50250243563736774, 8.947779886222148704 ) ) ;
#2266=CARTESIAN_POINT ( 'NONE',  ( -41.62287095715006302, -23.48783264082477729, -1.443836473390071928 ) ) ;
#2267=CARTESIAN_POINT ( 'NONE',  ( -119.5228709571500758, -29.50248528299804818, 1.056150453629045360 ) ) ;
#2268=B_SPLINE_CURVE_WITH_KNOTS ( 'NONE', 3,
 ( #23289, #40545, #71497, #56282 ),
 .UNSPECIFIED., .F., .F.,
 ( 4, 4 ),
 ( 0.000000000000000000, 1.000000000000000000 ),
 .UNSPECIFIED. ) ;
#2269=ORIENTED_EDGE ( 'NONE', *, *, #80574, .T. ) ;
#2273=B_SPLINE_CURVE_WITH_KNOTS ( 'NONE', 3,
 ( #76769, #54461, #69686, #7270, #44860, #22979 ),
 .UNSPECIFIED., .F., .F.,
 ( 4, 2, 4 ),
 ( 0.000000000000000000, 0.001380764517854766484, 0.002761529035709532967 ),
 .UNSPECIFIED. ) ;
#2274=VERTEX_POINT ( 'NONE', #8220 ) ;
#2277=CARTESIAN_POINT ( 'NONE',  ( -89.81226385320383088, -25.26364009184147008, 3.993462176398974162 ) ) ;
#2279=CARTESIAN_POINT ( 'NONE',  ( 16.23509277041898358, 12.58620111108425377, -1.500000000000002220 ) ) ;
#2283=CARTESIAN_POINT ( 'NONE',  ( -124.5228709571500616, -23.47596703998600631, 11.44779298504227860 ) ) ;
#2284=CARTESIAN_POINT ( 'NONE',  ( -18.97848940637192428, 11.77069306843248064, 11.49999999999998934 ) ) ;
#2285=CARTESIAN_POINT ( 'NONE',  ( -71.27197200528213727, -25.22889308749096315, 6.453605103024415257 ) ) ;
#2288=CARTESIAN_POINT ( 'NONE',  ( -101.6228709571500275, -23.73907113216992215, -1.053371485793222373 ) ) ;
#2290=CARTESIAN_POINT ( 'NONE',  ( -11.21968731015968856, -17.59241007644406096, 11.49999999999998934 ) ) ;
#2294=ORIENTED_EDGE ( 'NONE', *, *, #36548, .T. ) ;
#2295=CARTESIAN_POINT ( 'NONE',  ( -68.98049337452070517, -25.03149153121544757, 6.552244914804028930 ) ) ;
#2296=CARTESIAN_POINT ( 'NONE',  ( 19.40125262130244366, -8.172613994405130811, -1.500000000000002220 ) ) ;
#2299=DIRECTION ( 'NONE',  ( -0.000000000000000000, 2.173523156925979552E-06, -0.9999999999976378895 ) ) ;
#2301=CARTESIAN_POINT ( 'NONE',  ( -101.3347705957103528, -25.25419498530509443, 7.306917479324832598 ) ) ;
#2302=CARTESIAN_POINT ( 'NONE',  ( -60.62287095715004881, -24.99156045073392463, 7.747789690856161648 ) ) ;
#2303=CARTESIAN_POINT ( 'NONE',  ( -15.38093110518717666, 15.28219592669002402, -1.500000000000002220 ) ) ;
#2304=CARTESIAN_POINT ( 'NONE',  ( -117.6228709571500559, -23.47596703998600631, 11.44779298504227683 ) ) ;
#2305=CARTESIAN_POINT ( 'NONE',  ( -18.06118310651259407, 13.05043149098080058, 11.49999999999999645 ) ) ;
#2307=CARTESIAN_POINT ( 'NONE',  ( -51.11433842476665035, -25.24728772845527303, 5.424622507049278397 ) ) ;
#2308=CARTESIAN_POINT ( 'NONE',  ( 5.514125806255895004E-17, -29.50247984919044697, -1.443849411171584940 ) ) ;
#2310=AXIS2_PLACEMENT_3D ( 'NONE', #44803, #89474, #59529 ) ;
#2312=ORIENTED_EDGE ( 'NONE', *, *, #34316, .F. ) ;
#2313=ADVANCED_FACE ( 'NONE', ( #93946 ), #86343, .F. ) ;
#2315=ORIENTED_EDGE ( 'NONE', *, *, #76312, .T. ) ;
#2317=B_SPLINE_CURVE_WITH_KNOTS ( 'NONE', 3,
 ( #25292, #95310, #86693, #63890 ),
 .UNSPECIFIED., .F., .F.,
 ( 4, 4 ),
 ( 0.000000000000000000, 9.999999999998897304E-05 ),
 .UNSPECIFIED. ) ;
#2318=EDGE_CURVE ( 'NONE', #94960, #19028, #14417, .T. ) ;
#2319=CARTESIAN_POINT ( 'NONE',  ( 16.68447708738676383, -11.30049470069299922, -1.500000000000002220 ) ) ;
#2320=CARTESIAN_POINT ( 'NONE',  ( -105.5228709571500616, -25.00158670708909980, 2.256160236439166411 ) ) ;
#2321=ORIENTED_EDGE ( 'NONE', *, *, #88448, .F. ) ;
#2322=CARTESIAN_POINT ( 'NONE',  ( -130.5728709571500588, -25.26346845900570059, 3.135843962334224244 ) ) ;
#2323=CARTESIAN_POINT ( 'NONE',  ( -21.57557905285345612, -6.117077608415351087, -1.500000000000002220 ) ) ;
#2326=CARTESIAN_POINT ( 'NONE',  ( -34.62287095715004881, -23.48783264082478084, -1.443836473390074149 ) ) ;
#2327=CARTESIAN_POINT ( 'NONE',  ( -101.6270296092226602, -24.35071581493543746, 9.817618358456027039 ) ) ;
#2328=CARTESIAN_POINT ( 'NONE',  ( -110.5228709571500616, -25.00182538069145366, 7.747789668545101094 ) ) ;
#2329=CARTESIAN_POINT ( 'NONE',  ( -125.5228709571500616, -24.92579138211051060, 1.929029949967010271 ) ) ;
#2330=CARTESIAN_POINT ( 'NONE',  ( -97.24679607323146513, -24.75152770810920089, 1.363349870542269526 ) ) ;
#2331=CARTESIAN_POINT ( 'NONE',  ( -10.41718274906430786, -16.55731393670301088, 11.49999999999998934 ) ) ;
#2334=CARTESIAN_POINT ( 'NONE',  ( 19.32660459246815421, -9.429101867163046435, 11.49999999999998934 ) ) ;
#2335=CARTESIAN_POINT ( 'NONE',  ( -128.5557745493626669, -24.15543982623908548, -0.2315651400026392803 ) ) ;
#2336=CARTESIAN_POINT ( 'NONE',  ( -121.5228709571500758, -23.96127896941631974, -0.6493128931037975837 ) ) ;
#2338=CARTESIAN_POINT ( 'NONE',  ( -79.62287095715005592, -29.50247984919015209, -1.443849546365053582 ) ) ;
#2339=CARTESIAN_POINT ( 'NONE',  ( 4.748521865011817944, 22.44708532425888592, -1.500000000000002220 ) ) ;
#2342=CARTESIAN_POINT ( 'NONE',  ( -103.2228709571500644, -23.47596703998600631, 11.44779298504227860 ) ) ;
#2344=CARTESIAN_POINT ( 'NONE',  ( -3.374260732160392795, -19.82512954709321562, 11.49999999999999645 ) ) ;
#2348=CARTESIAN_POINT ( 'NONE',  ( -38.52287095715006870, -24.64965694238406613, 8.947790433994205372 ) ) ;
#2349=CARTESIAN_POINT ( 'NONE',  ( -85.62287095715004170, -24.91544648472620338, 1.928969306349226143 ) ) ;
#2350=CARTESIAN_POINT ( 'NONE',  ( 5.644138345009856117, 19.01542066204735448, -1.500000000000002220 ) ) ;
#2352=CARTESIAN_POINT ( 'NONE',  ( -68.93918693012690824, -25.25799956426409665, 6.184868438663939649 ) ) ;
#2353=CARTESIAN_POINT ( 'NONE',  ( 5.239555828037883778, -18.94419173073049478, -1.500000000000002220 ) ) ;
#2354=CARTESIAN_POINT ( 'NONE',  ( -42.50580221595909336, -23.96119346886880663, -0.6495511937831992544 ) ) ;
#2355=CARTESIAN_POINT ( 'NONE',  ( -58.62287095715004881, -23.48786465467241769, 11.44779295918254824 ) ) ;
#2357=DIRECTION ( 'NONE',  ( -3.773278334453079030E-23, 0.9999999999976377785, 2.173523156925979128E-06 ) ) ;
#2358=CARTESIAN_POINT ( 'NONE',  ( -20.42507745660439156, -2.452541965221147535, 11.49999999999999645 ) ) ;
#2359=DIRECTION ( 'NONE',  ( 1.000000000000000000, 3.773278334444166432E-23, 8.201307841325785021E-29 ) ) ;
#2362=CARTESIAN_POINT ( 'NONE',  ( 10.27952223434480494, 20.12118371629609470, 11.49999999999999645 ) ) ;
#2364=CARTESIAN_POINT ( 'NONE',  ( -69.34542366606198982, -25.12218970343129598, 6.299235195870870108 ) ) ;
#2365=CARTESIAN_POINT ( 'NONE',  ( -27.68651082257923690, -24.80976250947271211, 7.605672514646787619 ) ) ;
#2366=CARTESIAN_POINT ( 'NONE',  ( -100.6814946224345846, -25.31648867911425427, 5.043962003566639041 ) ) ;
#2367=EDGE_CURVE ( 'NONE', #51806, #6550, #9584, .T. ) ;
#2368=CARTESIAN_POINT ( 'NONE',  ( -27.12300167417273045, -24.93063615898261887, 8.164241745431031205 ) ) ;
#2371=ORIENTED_EDGE ( 'NONE', *, *, #12527, .F. ) ;
#2372=CARTESIAN_POINT ( 'NONE',  ( -80.31352994281894553, -25.31596222718856737, 4.969670813418835209 ) ) ;
#2373=CARTESIAN_POINT ( 'NONE',  ( -22.76716317511769461, -1.676022972194794791, -1.500000000000002220 ) ) ;
#2374=CARTESIAN_POINT ( 'NONE',  ( -111.1699275071095485, -25.23443226348169333, 3.685496250201802049 ) ) ;
#2375=CARTESIAN_POINT ( 'NONE',  ( -96.62356410278910346, -24.65952944569305316, 1.056160979905706121 ) ) ;
#2376=CARTESIAN_POINT ( 'NONE',  ( -82.63299475421938212, -24.15620529776628089, 10.23563542870660825 ) ) ;
#2378=CARTESIAN_POINT ( 'NONE',  ( 1.786768808452938950, -22.39398889530128756, 11.49999999999999645 ) ) ;
#2380=CARTESIAN_POINT ( 'NONE',  ( -49.62287095715005592, -29.50250786944525672, 11.44777988621624054 ) ) ;
#2381=CARTESIAN_POINT ( 'NONE',  ( -21.79611004543898289, 2.820803583321412678, -1.500000000000002220 ) ) ;
#2382=ADVANCED_FACE ( 'NONE', ( #48290 ), #18332, .F. ) ;
#2383=CARTESIAN_POINT ( 'NONE',  ( -126.1692003789631968, -25.31326721218303888, 3.500953664922433095 ) ) ;
#2384=CARTESIAN_POINT ( 'NONE',  ( -34.49701390240621635, -24.15620529776627379, 10.23563542870661003 ) ) ;
#2385=DIRECTION ( 'NONE',  ( 1.000000000000000000, 3.773278334444166432E-23, 8.201307841325785021E-29 ) ) ;
#2388=CARTESIAN_POINT ( 'NONE',  ( -112.5895376238167103, -24.66019654487199730, 8.947790411086121054 ) ) ;
#2389=ORIENTED_EDGE ( 'NONE', *, *, #55978, .F. ) ;
#2390=CARTESIAN_POINT ( 'NONE',  ( -17.91610926057384034, -10.00117247862695358, -1.500000000000002220 ) ) ;
#2392=ORIENTED_EDGE ( 'NONE', *, *, #91451, .F. ) ;
#2393=ORIENTED_EDGE ( 'NONE', *, *, #35572, .T. ) ;
#2394=EDGE_LOOP ( 'NONE', ( #40682, #37753, #79784, #70316 ) ) ;
#2396=CARTESIAN_POINT ( 'NONE',  ( 3.535601659403828201, -22.84449096179584160, -1.500000000000002220 ) ) ;
#2397=CARTESIAN_POINT ( 'NONE',  ( -41.52287095715005449, -24.66019654487198665, 8.947790411086121054 ) ) ;
#2399=B_SPLINE_CURVE_WITH_KNOTS ( 'NONE', 3,
 ( #69574, #47740, #23882, #32508 ),
 .UNSPECIFIED., .F., .F.,
 ( 4, 4 ),
 ( 0.000000000000000000, 0.0001000000000000028644 ),
 .UNSPECIFIED. ) ;
#2400=CARTESIAN_POINT ( 'NONE',  ( 12.22771034161782566, -16.27230226814707947, -1.500000000000002220 ) ) ;
#2401=VERTEX_POINT ( 'NONE', #64039 ) ;
#2403=CARTESIAN_POINT ( 'NONE',  ( -88.62287095715004170, -24.65952944569304606, 1.056160979905700570 ) ) ;
#2404=CARTESIAN_POINT ( 'NONE',  ( -46.62287095715004881, -24.65952944569304250, 1.056160979905693020 ) ) ;
#2406=CARTESIAN_POINT ( 'NONE',  ( -21.28347836979250118, 3.227085873532868021, 11.49999999999999645 ) ) ;
#2407=ORIENTED_EDGE ( 'NONE', *, *, #73948, .T. ) ;
#2408=CARTESIAN_POINT ( 'NONE',  ( -29.19847332116389538, -24.76881234832665868, 4.026236479318956896 ) ) ;
#2409=CARTESIAN_POINT ( 'NONE',  ( -49.26189073845563371, -25.31573744820669702, 4.538720682593869959 ) ) ;
#2410=EDGE_LOOP ( 'NONE', ( #14337, #78421, #68353, #8266 ) ) ;
#2411=B_SPLINE_CURVE_WITH_KNOTS ( 'NONE', 3,
 ( #10220, #11220, #88348, #41176 ),
 .UNSPECIFIED., .F., .F.,
 ( 4, 4 ),
 ( 0.000000000000000000, 9.999999999998897304E-05 ),
 .UNSPECIFIED. ) ;
#2412=CARTESIAN_POINT ( 'NONE',  ( 4.358738815032396907, -20.29635662749097236, 11.49999999999998934 ) ) ;
#2413=ORIENTED_EDGE ( 'NONE', *, *, #67881, .T. ) ;
#2414=CARTESIAN_POINT ( 'NONE',  ( -125.5569694553999085, -23.48783264082478794, -1.443836473390061936 ) ) ;
#2416=CARTESIAN_POINT ( 'NONE',  ( -82.62287095715005592, -24.64898659630367916, 1.056161002820826145 ) ) ;
#2417=CARTESIAN_POINT ( 'NONE',  ( -102.6228709571501128, -23.94994826722516379, -0.6494450866351678675 ) ) ;
#2418=ORIENTED_EDGE ( 'NONE', *, *, #96884, .T. ) ;
#2421=CARTESIAN_POINT ( 'NONE',  ( -123.6228709571500559, -24.64965695001469115, 8.947790433994175174 ) ) ;
#2423=CARTESIAN_POINT ( 'NONE',  ( 18.76863814860013235, 11.56883167669432133, 11.49999999999999645 ) ) ;
#2425=CARTESIAN_POINT ( 'NONE',  ( -103.6267870571919048, -24.34968618360933945, 0.1864209137778842229 ) ) ;
#2426=CARTESIAN_POINT ( 'NONE',  ( -19.94007547503736788, -10.58355046294204094, 11.49999999999998934 ) ) ;
#2427=CARTESIAN_POINT ( 'NONE',  ( -70.62287095715004170, -24.51163499207175889, 0.6490370598554249248 ) ) ;
#2429=VERTEX_POINT ( 'NONE', #95953 ) ;
#2432=EDGE_CURVE ( 'NONE', #98613, #76732, #77309, .T. ) ;
#2433=CARTESIAN_POINT ( 'NONE',  ( -94.52287095715006160, -24.64898659630367916, 1.056161002820827921 ) ) ;
#2435=CARTESIAN_POINT ( 'NONE',  ( -10.94853654022341516, 18.13385389444049522, 11.49999999999998934 ) ) ;
#2436=CARTESIAN_POINT ( 'NONE',  ( -61.52287095715006160, -29.50248528299804818, 1.056150453629034924 ) ) ;
#2437=CARTESIAN_POINT ( 'NONE',  ( -58.85672945663861810, -25.29489609436097552, 6.057563354383566967 ) ) ;
#2439=CARTESIAN_POINT ( 'NONE',  ( -80.62287095715004170, -24.15516710230296837, 10.28746687063728515 ) ) ;
#2440=CARTESIAN_POINT ( 'NONE',  ( -5.994446910899359438, -21.39327697068355505, -1.500000000000002220 ) ) ;
#2442=VECTOR ( 'NONE', #3286, 1000.000000000000114 ) ;
#2445=CARTESIAN_POINT ( 'NONE',  ( -85.62287095715005592, -29.50247984919015209, -1.443849546365051806 ) ) ;
#2446=CARTESIAN_POINT ( 'NONE',  ( -18.32239908988104204, -6.426282940459683068, 11.49999999999999645 ) ) ;
#2447=CARTESIAN_POINT ( 'NONE',  ( -40.62376381424373051, -25.11178338647325603, 2.840340238540807416 ) ) ;
#2448=B_SPLINE_CURVE_WITH_KNOTS ( 'NONE', 3,
 ( #77304, #8814, #16407, #37760, #15410, #7806 ),
 .UNSPECIFIED., .F., .F.,
 ( 4, 2, 4 ),
 ( 1.570887131794795405E-05, 0.001396322306279762808, 0.002776935741241577573 ),
 .UNSPECIFIED. ) ;
#2450=CARTESIAN_POINT ( 'NONE',  ( 8.918240691521024388, 17.32521578647535776, 11.49999999999998934 ) ) ;
#2451=CARTESIAN_POINT ( 'NONE',  ( -0.4629837013611828866, -21.40787533109759977, 11.49999999999998934 ) ) ;
#2452=CARTESIAN_POINT ( 'NONE',  ( -32.58953762381671737, -24.64965694238406613, 8.947790433994661896 ) ) ;
#2454=CARTESIAN_POINT ( 'NONE',  ( -51.58729945987563070, -24.34968618360933590, 0.1864209137778788938 ) ) ;
#2455=LINE ( 'NONE', #33389, #63862 ) ;
#2456=CARTESIAN_POINT ( 'NONE',  ( 5.860688371469950475, 21.97560254587667217, -1.500000000000002220 ) ) ;
#2457=EDGE_CURVE ( 'NONE', #15382, #81082, #54337, .T. ) ;
#2459=CARTESIAN_POINT ( 'NONE',  ( -106.5889851739996317, -24.35071581493544457, 9.817618358456019934 ) ) ;
#2460=CARTESIAN_POINT ( 'NONE',  ( -80.52287095715009002, -24.14321612903115977, -0.2833117244521555222 ) ) ;
#2461=CARTESIAN_POINT ( 'NONE',  ( -18.69216024341242743, -6.879743215651725308, 11.49999999999999645 ) ) ;
#2463=EDGE_CURVE ( 'NONE', #68328, #44325, #13157, .T. ) ;
#2466=ORIENTED_EDGE ( 'NONE', *, *, #79934, .T. ) ;
#2467=CARTESIAN_POINT ( 'NONE',  ( -96.62287095715005592, -23.47596703998600631, 11.44779298504227860 ) ) ;
#2468=CARTESIAN_POINT ( 'NONE',  ( -31.81571590327885701, -25.16202561908117730, 2.791798636425737445 ) ) ;
#2470=CARTESIAN_POINT ( 'NONE',  ( -6.994818212361641585, 20.52682044044541598, 11.49999999999998934 ) ) ;
#2471=EDGE_CURVE ( 'NONE', #44562, #991, #72134, .T. ) ;
#2472=FACE_OUTER_BOUND ( 'NONE', #9381, .T. ) ;
#2473=CARTESIAN_POINT ( 'NONE',  ( -7.634514033349506512, -17.95459398628807435, -1.500000000000002220 ) ) ;
#2474=EDGE_CURVE ( 'NONE', #32256, #75656, #2411, .T. ) ;
#2476=ORIENTED_EDGE ( 'NONE', *, *, #669, .F. ) ;
#2479=CARTESIAN_POINT ( 'NONE',  ( -16.75749313124890350, -11.57646860041911019, 11.49999999999999645 ) ) ;
#2480=CARTESIAN_POINT ( 'NONE',  ( -85.62287095715005592, -23.47593901973091235, -1.443836447539002865 ) ) ;
#2482=ORIENTED_EDGE ( 'NONE', *, *, #68508, .F. ) ;
#2484=FACE_OUTER_BOUND ( 'NONE', #4222, .T. ) ;
#2487=B_SPLINE_CURVE_WITH_KNOTS ( 'NONE', 3,
 ( #14077, #15578, #38923, #30813, #69877, #45055 ),
 .UNSPECIFIED., .F., .F.,
 ( 4, 2, 4 ),
 ( 6.384118678613282972E-06, 0.001386860460828377370, 0.002767336802978141459 ),
 .UNSPECIFIED. ) ;
#2490=CARTESIAN_POINT ( 'NONE',  ( -109.5495869374086766, -24.65952944569305316, 1.056160979905708786 ) ) ;
#2493=CARTESIAN_POINT ( 'NONE',  ( 9.743704349311032686, 20.77413290702584092, 11.49999999999999645 ) ) ;
#2494=CARTESIAN_POINT ( 'NONE',  ( 15.01325480956343483, 17.08929600257393489, -1.500000000000002220 ) ) ;
#2495=CARTESIAN_POINT ( 'NONE',  ( -71.25764098586252260, -25.11044779094143564, 7.228272730454482264 ) ) ;
#2497=FACE_OUTER_BOUND ( 'NONE', #37706, .T. ) ;
#2498=B_SPLINE_CURVE_WITH_KNOTS ( 'NONE', 3,
 ( #66699, #97610, #68167, #59568, #43343, #90500 ),
 .UNSPECIFIED., .F., .F.,
 ( 4, 2, 4 ),
 ( 6.384118678617895914E-06, 0.001386860460828379105, 0.002767336802978140591 ),
 .UNSPECIFIED. ) ;
#2499=CARTESIAN_POINT ( 'NONE',  ( -69.74074321433934642, -25.16191154851385292, 6.930438937598965232 ) ) ;
#2500=AXIS2_PLACEMENT_3D ( 'NONE', #91333, #28432, #51788 ) ;
#2501=CARTESIAN_POINT ( 'NONE',  ( -15.17958814119055155, -15.74432251006154715, 11.49999999999998934 ) ) ;
#2502=EDGE_CURVE ( 'NONE', #71172, #88549, #3619, .T. ) ;
#2503=CARTESIAN_POINT ( 'NONE',  ( -69.60238590130140324, -23.73791477778911840, 11.05961554403170766 ) ) ;
#2505=FACE_OUTER_BOUND ( 'NONE', #74403, .T. ) ;
#2507=CARTESIAN_POINT ( 'NONE',  ( -58.51506555621022443, -23.73766607897670156, -1.055555164236457344 ) ) ;
#2509=CARTESIAN_POINT ( 'NONE',  ( -17.38880980700008294, 10.71821138944157603, -1.500000000000002220 ) ) ;
#2510=EDGE_LOOP ( 'NONE', ( #70510, #86748, #31405, #29446 ) ) ;
#2511=ORIENTED_EDGE ( 'NONE', *, *, #21904, .F. ) ;
#2512=CARTESIAN_POINT ( 'NONE',  ( 3.792298468851710069, -22.70151372599487871, -1.500000000000002220 ) ) ;
#2521=ADVANCED_FACE ( 'NONE', ( #6600 ), #43670, .F. ) ;
#2522=CARTESIAN_POINT ( 'NONE',  ( -78.58953762381672448, -24.64965694238407679, 8.947790433994653014 ) ) ;
#2524=CARTESIAN_POINT ( 'NONE',  ( 20.09692647535021948, 7.048664716645152595, 11.49999999999999645 ) ) ;
#2525=VERTEX_POINT ( 'NONE', #21310 ) ;
#2526=VERTEX_POINT ( 'NONE', #27944 ) ;
#2527=CARTESIAN_POINT ( 'NONE',  ( -5.994446910899359438, -21.39327697068355505, 11.49999999999998934 ) ) ;
#2528=CARTESIAN_POINT ( 'NONE',  ( 13.18972694569024640, 15.87703813876158598, -1.500000000000002220 ) ) ;
#2529=VERTEX_POINT ( 'NONE', #52282 ) ;
#2531=CARTESIAN_POINT ( 'NONE',  ( -93.52287095715006160, -29.50248528299804818, 1.056150453629040253 ) ) ;
#2532=VERTEX_POINT ( 'NONE', #5100 ) ;
#2533=CARTESIAN_POINT ( 'NONE',  ( -62.62287095715004881, -29.50250786944525672, 11.44777988621623876 ) ) ;
#2534=ORIENTED_EDGE ( 'NONE', *, *, #59401, .F. ) ;
#2535=CARTESIAN_POINT ( 'NONE',  ( -58.53402618834690685, -24.66019654487199730, 8.947790411086117501 ) ) ;
#2536=CARTESIAN_POINT ( 'NONE',  ( -71.29839951630819428, -25.23282476250683004, 6.331943296452392289 ) ) ;
#2537=CARTESIAN_POINT ( 'NONE',  ( -17.14161228048114438, 11.91956482804130601, -1.500000000000002220 ) ) ;
#2538=CARTESIAN_POINT ( 'NONE',  ( -11.22809577558575000, 18.72649003030000259, 11.49999999999999645 ) ) ;
#2539=CARTESIAN_POINT ( 'NONE',  ( -26.64126777428346315, -24.77993686738184209, 7.094644171777847674 ) ) ;
#2541=CARTESIAN_POINT ( 'NONE',  ( -9.984083066403742990, 20.14924292131567185, -1.500000000000002220 ) ) ;
#2542=CARTESIAN_POINT ( 'NONE',  ( 5.579783289733251550, -20.15082174716252794, -1.500000000000002220 ) ) ;
#2543=CARTESIAN_POINT ( 'NONE',  ( -26.31589504439661198, -24.88149045850647312, 6.467908346933119113 ) ) ;
#2544=CARTESIAN_POINT ( 'NONE',  ( -57.62287095715004170, -24.33832256526968862, 0.1851278514119866214 ) ) ;
#2546=ORIENTED_EDGE ( 'NONE', *, *, #49910, .F. ) ;
#2547=AXIS2_PLACEMENT_3D ( 'NONE', #26445, #96445, #48282 ) ;
#2548=ORIENTED_EDGE ( 'NONE', *, *, #60712, .F. ) ;
#2549=VERTEX_POINT ( 'NONE', #89839 ) ;
#2550=CARTESIAN_POINT ( 'NONE',  ( -52.63895471842339902, -24.15543982623907482, -0.2315651400026529916 ) ) ;
#2552=CARTESIAN_POINT ( 'NONE',  ( 12.64048258313813733, 17.25876517447949610, -1.500000000000002220 ) ) ;
#2553=CARTESIAN_POINT ( 'NONE',  ( -4.763361739610138201, -21.85411462188651299, 11.49999999999999645 ) ) ;
#2555=CARTESIAN_POINT ( 'NONE',  ( -95.52287095715004739, -23.47593901973090169, -1.443836447538996648 ) ) ;
#2556=CARTESIAN_POINT ( 'NONE',  ( 13.75562813033083742, -15.94169299924578453, -1.500000000000002220 ) ) ;
#2557=CARTESIAN_POINT ( 'NONE',  ( -30.55797716464545744, -24.27484564323477656, 9.960304333224314632 ) ) ;
#2558=CARTESIAN_POINT ( 'NONE',  ( -15.73602684802347440, -12.20685706852216867, -1.500000000000002220 ) ) ;
#2560=( BOUNDED_SURFACE ( )  B_SPLINE_SURFACE ( 3, 1, ( 
 ( #75581, #83704 ),
 ( #14690, #76579 ),
 ( #14185, #22786 ),
 ( #5587, #77081 ),
 ( #38532, #45162 ),
 ( #7083, #76086 ),
 ( #38034, #6084 ),
 ( #83199, #84701 ),
 ( #90824, #37539 ),
 ( #30418, #15192 ),
 ( #52269, #67499 ),
 ( #68983, #30918 ),
 ( #99907, #68489 ),
 ( #61888, #61389 ),
 ( #51773, #70491 ),
 ( #94314, #25305 ),
 ( #54278, #72001 ),
 ( #974, #31928 ),
 ( #24800, #86210 ),
 ( #469, #55780 ) ),
 .UNSPECIFIED., .F., .F., .T. ) 
 B_SPLINE_SURFACE_WITH_KNOTS ( ( 4, 3, 1, 1, 3, 3, 1, 1, 3, 4 ),
 ( 2, 2 ),
 ( 0.000000000000000000, 0.1255889732084984889, 0.1669421422606964800, 0.2082953113128944711, 0.2496484803650923512, 0.7477322152634136021, 0.7890853843156119263, 0.8304385533678104725, 0.8717917224200087967, 1.000000000000000000 ),
 ( 0.000000000000000000, 1.000000000000000000 ),
 .UNSPECIFIED. ) 
 GEOMETRIC_REPRESENTATION_ITEM ( )  RATIONAL_B_SPLINE_SURFACE ( (
 ( 0.9999602609241470264, 0.9999602609241470264),
 ( 0.9987387818499366965, 0.9987387818499366965),
 ( 0.9998573533027315108, 0.9998573533027315108),
 ( 1.003315975282531802, 1.003315975282531802),
 ( 1.003315975282531802, 1.003315975282531802),
 ( 1.003315975282531802, 1.003315975282531802),
 ( 1.003315975282531802, 1.003315975282531802),
 ( 1.003315975282531802, 1.003315975282531802),
 ( 1.003315975282531802, 1.003315975282531802),
 ( 0.9773170091682806815, 0.9773170091682806815),
 ( 0.9773170091682806815, 0.9773170091682806815),
 ( 1.003315975282531802, 1.003315975282531802),
 ( 1.003315975282531802, 1.003315975282531802),
 ( 1.003315975282531802, 1.003315975282531802),
 ( 1.003315975282531802, 1.003315975282531802),
 ( 1.003315975282531802, 1.003315975282531802),
 ( 1.003315975282531802, 1.003315975282531802),
 ( 0.9997852197113853423, 0.9997852197113853423),
 ( 0.9986931415022445302, 0.9986931415022445302),
 ( 1.000039740655109810, 1.000039740655109810) ) ) 
 REPRESENTATION_ITEM ( '' )  SURFACE ( )  );
#2561=FACE_OUTER_BOUND ( 'NONE', #11599, .T. ) ;
#2562=CARTESIAN_POINT ( 'NONE',  ( -35.52287095715006870, -23.48786465467240347, 11.44779295918255180 ) ) ;
#2563=CARTESIAN_POINT ( 'NONE',  ( 3.837975233861466329, 21.70421690940786874, -1.500000000000002220 ) ) ;
#2565=CARTESIAN_POINT ( 'NONE',  ( -65.50511328601497496, -24.15602025860896518, 10.28564288303534724 ) ) ;
#2567=CARTESIAN_POINT ( 'NONE',  ( -30.64752034897746924, -23.47593901973090169, -1.443836447538997758 ) ) ;
#2568=CARTESIAN_POINT ( 'NONE',  ( -28.39957058925135414, -24.99626215692908815, 7.214475432169975555 ) ) ;
#2569=CARTESIAN_POINT ( 'NONE',  ( -25.78500995861852019, -24.78937058933301785, 3.117906490743990844 ) ) ;
#2570=CARTESIAN_POINT ( 'NONE',  ( -61.58953762381672448, -24.65952944569304606, 1.056160979905703234 ) ) ;
#2571=CARTESIAN_POINT ( 'NONE',  ( -21.20786952941880443, -2.223526401999901925, 11.49999999999998934 ) ) ;
#2573=CARTESIAN_POINT ( 'NONE',  ( -66.55620429048340725, -23.47596703998600276, 11.44779298504227505 ) ) ;
#2575=CARTESIAN_POINT ( 'NONE',  ( -67.52287095715006160, -24.66019654487199730, 8.947790411086115725 ) ) ;
#2576=CARTESIAN_POINT ( 'NONE',  ( -21.83012794225054165, -5.757306806698124113, -1.500000000000002220 ) ) ;
#2577=B_SPLINE_CURVE_WITH_KNOTS ( 'NONE', 3,
 ( #12877, #52460, #36236, #83393 ),
 .UNSPECIFIED., .F., .F.,
 ( 4, 4 ),
 ( 6.699507672488401150E-09, 0.001652437988939160470 ),
 .UNSPECIFIED. ) ;
#2584=CARTESIAN_POINT ( 'NONE',  ( -31.58666371736434186, -24.35071581493542325, 9.817618358456039473 ) ) ;
#2585=CARTESIAN_POINT ( 'NONE',  ( 19.63295818312489871, -1.572306604260808260, 11.49999999999999645 ) ) ;
#2588=CARTESIAN_POINT ( 'NONE',  ( -73.52287095715007581, -23.47596703998600631, 11.44779298504228748 ) ) ;
#2591=CARTESIAN_POINT ( 'NONE',  ( -99.62531270275181328, -24.51314013834316796, 0.6176544820404258340 ) ) ;
#2593=CARTESIAN_POINT ( 'NONE',  ( -124.5222546785644511, -23.48786465467241769, 11.44779295918253581 ) ) ;
#2596=DIRECTION ( 'NONE',  ( 0.000000000000000000, -0.9999999999976377785, -2.173523156925979975E-06 ) ) ;
#2601=CARTESIAN_POINT ( 'NONE',  ( -17.60924879254659459, 8.996216891746938060, -1.500000000000002220 ) ) ;
#2602=ORIENTED_EDGE ( 'NONE', *, *, #36144, .T. ) ;
#2604=CARTESIAN_POINT ( 'NONE',  ( 6.697674113365701842, 19.09646837838083400, 11.49999999999999645 ) ) ;
#2606=EDGE_LOOP ( 'NONE', ( #52711, #5403, #87763, #39318 ) ) ;
#2609=CARTESIAN_POINT ( 'NONE',  ( -51.26639007284612148, -25.29356494163747371, 5.550358426643942522 ) ) ;
#2612=CARTESIAN_POINT ( 'NONE',  ( -32.38277616518237778, -25.11010177982458913, 2.831122766525575596 ) ) ;
#2613=CARTESIAN_POINT ( 'NONE',  ( -18.22994410263883225, 8.285605901428201747, -1.500000000000002220 ) ) ;
#2614=EDGE_CURVE ( 'NONE', #11989, #72199, #99047, .T. ) ;
#2618=CARTESIAN_POINT ( 'NONE',  ( -51.52287095715006160, -24.34917612406836795, 0.1852690917426518535 ) ) ;
#2619=DIRECTION ( 'NONE',  ( 0.000000000000000000, -0.9999999999976377785, -2.173523156925979975E-06 ) ) ;
#2622=CARTESIAN_POINT ( 'NONE',  ( -101.6533370195574690, -25.22562951682090215, 3.608687682288769238 ) ) ;
#2623=ADVANCED_FACE ( 'NONE', ( #90337 ), #81730, .F. ) ;
#2625=CARTESIAN_POINT ( 'NONE',  ( -101.9685402542758510, -25.30060005375480614, 6.009289253917324380 ) ) ;
#2626=ORIENTED_EDGE ( 'NONE', *, *, #36952, .F. ) ;
#2627=CARTESIAN_POINT ( 'NONE',  ( 11.02309159617336221, -17.05227643984133934, -1.500000000000002220 ) ) ;
#2630=CARTESIAN_POINT ( 'NONE',  ( -122.5228709571501042, -23.73907113216990439, -1.053371485793246132 ) ) ;
#2632=CARTESIAN_POINT ( 'NONE',  ( -59.50896880679595569, -23.96169478059712787, 10.65365249895718769 ) ) ;
#2636=CARTESIAN_POINT ( 'NONE',  ( -99.62287095715005592, -29.50248528299804818, 1.056150453629042030 ) ) ;
#2637=CARTESIAN_POINT ( 'NONE',  ( -16.97324839047195866, 12.58421825509937442, 11.49999999999999645 ) ) ;
#2638=CARTESIAN_POINT ( 'NONE',  ( -9.153499762860807465, 20.15527781828815534, 11.49999999999998934 ) ) ;
#2639=EDGE_CURVE ( 'NONE', #66840, #909, #75594, .T. ) ;
#2640=CARTESIAN_POINT ( 'NONE',  ( -17.20787902393383462, -11.26661214947554157, -1.500000000000002220 ) ) ;
#2641=VECTOR ( 'NONE', #96333, 1000.000000000000114 ) ;
#2643=CARTESIAN_POINT ( 'NONE',  ( -94.52287095715010423, -24.35013146730204170, 9.818937971375104823 ) ) ;
#2644=ORIENTED_EDGE ( 'NONE', *, *, #50963, .F. ) ;
#2645=CARTESIAN_POINT ( 'NONE',  ( -113.6228709571500559, -29.50250786944525672, 11.44777988621622988 ) ) ;
#2646=CARTESIAN_POINT ( 'NONE',  ( -85.62287095715005592, -23.48786465467241413, 11.44779295918254114 ) ) ;
#2648=AXIS2_PLACEMENT_3D ( 'NONE', #42589, #12617, #73035 ) ;
#2649=VERTEX_POINT ( 'NONE', #12703 ) ;
#2650=AXIS2_PLACEMENT_3D ( 'NONE', #4041, #97864, #74538 ) ;
#2652=CARTESIAN_POINT ( 'NONE',  ( -64.62287095715005592, -29.50250786944525672, 11.44777988621623876 ) ) ;
#2653=CARTESIAN_POINT ( 'NONE',  ( -110.6228709571500559, -29.50250786944525672, 11.44777988621622988 ) ) ;
#2655=CARTESIAN_POINT ( 'NONE',  ( -14.15296684469643118, 15.14645709676483420, -1.500000000000002220 ) ) ;
#2656=VECTOR ( 'NONE', #76179, 1000.000000000000114 ) ;
#2657=CARTESIAN_POINT ( 'NONE',  ( -21.58526226860004371, 1.989002153404973328, 11.49999999999999645 ) ) ;
#2658=ORIENTED_EDGE ( 'NONE', *, *, #34891, .T. ) ;
#2659=CARTESIAN_POINT ( 'NONE',  ( -69.75867330073758410, -25.13524716939983961, 2.913775892772168419 ) ) ;
#2660=DIRECTION ( 'NONE',  ( -3.773278334453079030E-23, 0.9999999999976377785, 2.173523156925979128E-06 ) ) ;
#2661=CARTESIAN_POINT ( 'NONE',  ( -4.914914792326205983, -21.87198836336805385, 11.49999999999998934 ) ) ;
#2664=CARTESIAN_POINT ( 'NONE',  ( -57.92287095715004597, -23.47596703998600276, 11.44779298504227860 ) ) ;
#2665=ORIENTED_EDGE ( 'NONE', *, *, #85089, .F. ) ;
#2669=EDGE_LOOP ( 'NONE', ( #16007, #37598, #18262, #85035 ) ) ;
#2670=CARTESIAN_POINT ( 'NONE',  ( -46.53036571332072668, -24.66019654487199375, 8.947790411086122830 ) ) ;
#2671=VERTEX_POINT ( 'NONE', #74606 ) ;
#2673=CARTESIAN_POINT ( 'NONE',  ( 15.87343765641381665, 14.11872912734625274, -1.500000000000002220 ) ) ;
#2675=CARTESIAN_POINT ( 'NONE',  ( -68.62287095715004170, -23.73907113216991860, -1.053371485793230367 ) ) ;
#2676=CARTESIAN_POINT ( 'NONE',  ( 15.22768361601695020, -15.61070304372801587, -1.500000000000002220 ) ) ;
#2677=FACE_OUTER_BOUND ( 'NONE', #26501, .T. ) ;
#2678=CARTESIAN_POINT ( 'NONE',  ( -107.5228709571500332, -23.94994826722564696, -0.6494450866342712514 ) ) ;
#2680=CARTESIAN_POINT ( 'NONE',  ( -20.57654891367511851, 7.437132321665034240, -1.500000000000002220 ) ) ;
#2682=ORIENTED_EDGE ( 'NONE', *, *, #73080, .F. ) ;
#2683=CARTESIAN_POINT ( 'NONE',  ( -108.8968792378191921, -29.50249917535260380, 7.447779886225679213 ) ) ;
#2684=CARTESIAN_POINT ( 'NONE',  ( -48.87675733776060838, -25.26337330288447092, 6.266175371071904365 ) ) ;
#2688=ORIENTED_EDGE ( 'NONE', *, *, #100417, .T. ) ;
#2691=CARTESIAN_POINT ( 'NONE',  ( 21.23515499356076930, 0.7789969333488580006, 11.49999999999998934 ) ) ;
#2694=DIRECTION ( 'NONE',  ( -1.000000000000000000, -3.773278334444167608E-23, -8.201307833595939069E-29 ) ) ;
#2695=B_SPLINE_CURVE_WITH_KNOTS ( 'NONE', 3,
 ( #97751, #82032, #88655, #89644 ),
 .UNSPECIFIED., .F., .F.,
 ( 4, 4 ),
 ( 1.387778780781445521E-17, 9.999999999996123101E-05 ),
 .UNSPECIFIED. ) ;
#2696=CARTESIAN_POINT ( 'NONE',  ( -68.63109341914197614, -24.34968618360933590, 0.1864209137778813363 ) ) ;
#2697=CARTESIAN_POINT ( 'NONE',  ( -18.68671320864135765, 5.291888989699490509, 11.49999999999998934 ) ) ;
#2698=CARTESIAN_POINT ( 'NONE',  ( -45.57565279233343603, -24.92564183028979130, 1.928384488918256645 ) ) ;
#2701=CARTESIAN_POINT ( 'NONE',  ( -18.49313839071750820, -6.238557295281221826, 11.49999999999999645 ) ) ;
#2703=EDGE_CURVE ( 'NONE', #39193, #923, #57935, .T. ) ;
#2708=CARTESIAN_POINT ( 'NONE',  ( -89.63160522007152053, -24.15543982623907482, -0.2315651400026483009 ) ) ;
#2709=EDGE_CURVE ( 'NONE', #59212, #24964, #56680, .T. ) ;
#2712=CARTESIAN_POINT ( 'NONE',  ( -81.01753736565918018, -25.24813972518663618, 7.476685482214374900 ) ) ;
#2713=CARTESIAN_POINT ( 'NONE',  ( -2.223759785643201869, -19.53228827767608777, -1.500000000000002220 ) ) ;
#2716=CARTESIAN_POINT ( 'NONE',  ( -43.55620429048339304, -24.64898659630528854, 1.056161002820822592 ) ) ;
#2719=ADVANCED_FACE ( 'NONE', ( #86225 ), #77335, .T. ) ;
#2723=CARTESIAN_POINT ( 'NONE',  ( -97.54592273218207765, -24.66019654487199730, 8.947790411086115725 ) ) ;
#2724=LINE ( 'NONE', #33664, #12843 ) ;
#2727=CARTESIAN_POINT ( 'NONE',  ( -69.36083545395123906, -25.31201746261485752, 6.029876604266336315 ) ) ;
#2729=CARTESIAN_POINT ( 'NONE',  ( -12.53609265798794681, -15.47265773855268378, -1.500000000000002220 ) ) ;
#2730=B_SPLINE_CURVE_WITH_KNOTS ( 'NONE', 3,
 ( #18879, #95510, #66592, #96505, #25497, #11766, #81284, #42253, #80285, #10779 ),
 .UNSPECIFIED., .F., .F.,
 ( 4, 2, 2, 2, 4 ),
 ( 0.000000000000000000, 0.0002024578457012554070, 0.0004049156914025108141, 0.0006073735371037662211, 0.0008098313828050216281 ),
 .UNSPECIFIED. ) ;
#2731=CARTESIAN_POINT ( 'NONE',  ( -75.62528596432828465, -24.92592662359561473, 8.075495903018000021 ) ) ;
#2732=CARTESIAN_POINT ( 'NONE',  ( -16.51628311069853083, -11.03946451426814690, -1.500000000000002220 ) ) ;
#2735=CARTESIAN_POINT ( 'NONE',  ( -120.5895376238167103, -23.48783264082479505, -1.443836473390058384 ) ) ;
#2736=DIRECTION ( 'NONE',  ( -1.000000000000000000, -3.773278334444166432E-23, -8.201307841325785021E-29 ) ) ;
#2739=CARTESIAN_POINT ( 'NONE',  ( 20.50115541507891948, 3.495740877612329101, 11.49999999999999645 ) ) ;
#2740=CARTESIAN_POINT ( 'NONE',  ( -38.22287095715005734, -23.47593901973090169, -1.443836447538997980 ) ) ;
#2741=CARTESIAN_POINT ( 'NONE',  ( -62.52287095715006160, -23.47596703998600631, 11.44779298504228926 ) ) ;
#2742=CARTESIAN_POINT ( 'NONE',  ( -12.33899560737860313, 19.21699747222852395, 11.49999999999999645 ) ) ;
#2743=EDGE_LOOP ( 'NONE', ( #38964, #69432, #64951, #10772 ) ) ;
#2744=DIRECTION ( 'NONE',  ( -0.000000000000000000, 2.173523156925979552E-06, -0.9999999999976378895 ) ) ;
#2746=ORIENTED_EDGE ( 'NONE', *, *, #35016, .T. ) ;
#2747=CARTESIAN_POINT ( 'NONE',  ( -10.81679630089563915, -17.07601267366916886, 11.49999999999998934 ) ) ;
#2750=AXIS2_PLACEMENT_3D ( 'NONE', #100199, #60191, #53579 ) ;
#2751=CARTESIAN_POINT ( 'NONE',  ( -100.6228709571499991, -24.15431212366392089, -0.2830839119429089390 ) ) ;
#2752=EDGE_CURVE ( 'NONE', #79650, #40077, #54791, .T. ) ;
#2753=EDGE_LOOP ( 'NONE', ( #12243, #42485, #15967, #43095 ) ) ;
#2754=CARTESIAN_POINT ( 'NONE',  ( -70.62287095715005592, -24.99156045073392463, 7.747789690856161648 ) ) ;
#2755=CARTESIAN_POINT ( 'NONE',  ( -100.6228709571500559, -23.47593901973091235, -1.443836447539001089 ) ) ;
#2756=CARTESIAN_POINT ( 'NONE',  ( -8.782848147209532996, 18.00178819457707746, -1.500000000000002220 ) ) ;
#2757=CARTESIAN_POINT ( 'NONE',  ( 11.42219733811748306, 17.55150860717643724, 11.49999999999999645 ) ) ;
#2759=CARTESIAN_POINT ( 'NONE',  ( -27.70544111104076990, -24.65058036537550024, 8.251826706788236265 ) ) ;
#2761=CARTESIAN_POINT ( 'NONE',  ( 3.837975233861466329, 21.70421690940786874, 11.49999999999998934 ) ) ;
#2763=CARTESIAN_POINT ( 'NONE',  ( -40.41683116089613748, -25.27806106706002964, 5.082404452749530677 ) ) ;
#2764=ORIENTED_EDGE ( 'NONE', *, *, #68567, .F. ) ;
#2766=CARTESIAN_POINT ( 'NONE',  ( -60.52287095715006160, -23.47593901973090169, -1.443836447538996870 ) ) ;
#2768=CARTESIAN_POINT ( 'NONE',  ( -72.62691918628158305, -24.51314013834316796, 0.6176544820404145097 ) ) ;
#2769=VERTEX_POINT ( 'NONE', #55295 ) ;
#2771=B_SPLINE_CURVE_WITH_KNOTS ( 'NONE', 3,
 ( #23018, #85944, #92051, #30656 ),
 .UNSPECIFIED., .F., .F.,
 ( 4, 4 ),
 ( 0.9604717738612708056, 0.9694782051333865613 ),
 .UNSPECIFIED. ) ;
#2772=ORIENTED_EDGE ( 'NONE', *, *, #50805, .F. ) ;
#2773=ORIENTED_EDGE ( 'NONE', *, *, #100154, .F. ) ;
#2774=CARTESIAN_POINT ( 'NONE',  ( -83.52287095715006160, -23.47596703998600631, 11.44779298504228571 ) ) ;
#2776=CARTESIAN_POINT ( 'NONE',  ( -58.62287095715004881, -23.48783264082478439, -1.443836473390069264 ) ) ;
#2777=CARTESIAN_POINT ( 'NONE',  ( 18.81462172601333549, -8.267562025728075525, -1.500000000000002220 ) ) ;
#2782=CARTESIAN_POINT ( 'NONE',  ( -6.278373996654322831, -21.41630973362384083, 11.49999999999998934 ) ) ;
#2784=CARTESIAN_POINT ( 'NONE',  ( -70.80335600588159650, -25.15073531561621323, 6.999027372372252920 ) ) ;
#2789=CARTESIAN_POINT ( 'NONE',  ( 15.14581745102402088, -14.33592658440916523, 11.49999999999998934 ) ) ;
#2791=B_SPLINE_CURVE_WITH_KNOTS ( 'NONE', 3,
 ( #17247, #30473, #70036, #62435 ),
 .UNSPECIFIED., .F., .F.,
 ( 4, 4 ),
 ( 0.000000000000000000, 0.002134615384615401457 ),
 .UNSPECIFIED. ) ;
#2793=ORIENTED_EDGE ( 'NONE', *, *, #34831, .F. ) ;
#2796=CARTESIAN_POINT ( 'NONE',  ( -32.82969853631264101, -25.04397465799123168, 2.466842825816077944 ) ) ;
#2797=CARTESIAN_POINT ( 'NONE',  ( -9.798014431990228701, 18.61115389415964572, -1.500000000000002220 ) ) ;
#2800=CARTESIAN_POINT ( 'NONE',  ( -114.5562042904833930, -23.48783264082478794, -1.443836473390060604 ) ) ;
#2802=CARTESIAN_POINT ( 'NONE',  ( -120.5186613917142182, -24.40133493613049964, 9.663955038902800609 ) ) ;
#2803=VECTOR ( 'NONE', #82415, 1000.000000000000114 ) ;
#2804=CARTESIAN_POINT ( 'NONE',  ( -86.58307941256070706, -24.66019654487200086, 8.947790411086115725 ) ) ;
#2805=CARTESIAN_POINT ( 'NONE',  ( -49.52287095715006160, -24.64898659630367561, 1.056161002820821038 ) ) ;
#2806=CARTESIAN_POINT ( 'NONE',  ( 12.82194709444435077, -17.51738216156474337, -1.500000000000002220 ) ) ;
#2807=CARTESIAN_POINT ( 'NONE',  ( -57.52287095715007581, -24.51283580621365132, 0.6167428607019714848 ) ) ;
#2808=CARTESIAN_POINT ( 'NONE',  ( 11.91227609878784399, -18.80521639033699799, 11.49999999999999645 ) ) ;
#2810=CARTESIAN_POINT ( 'NONE',  ( -51.44586644541745812, -25.24728857774910296, 5.815367749938357811 ) ) ;
#2812=CARTESIAN_POINT ( 'NONE',  ( -79.11611000704996854, -29.50249039766296022, 3.409318347773680369 ) ) ;
#2817=CARTESIAN_POINT ( 'NONE',  ( -122.6228709571500417, -29.50250243563736774, 8.947779886222134493 ) ) ;
#2818=CARTESIAN_POINT ( 'NONE',  ( -35.52287095715006870, -24.99132157543083821, 2.256160258750667502 ) ) ;
#2820=VERTEX_POINT ( 'NONE', #92328 ) ;
#2822=CARTESIAN_POINT ( 'NONE',  ( -42.62287095715007013, -24.35013146730202394, 9.818937971375111928 ) ) ;
#2823=CARTESIAN_POINT ( 'NONE',  ( 5.309366582633749054, -21.77581755331916824, -1.500000000000002220 ) ) ;
#2824=ORIENTED_EDGE ( 'NONE', *, *, #97108, .T. ) ;
#2826=CARTESIAN_POINT ( 'NONE',  ( -34.52287095715006870, -24.50321055353803956, 9.387540953477520489 ) ) ;
#2828=EDGE_CURVE ( 'NONE', #30682, #36801, #11912, .T. ) ;
#2829=CARTESIAN_POINT ( 'NONE',  ( -39.44890538690540893, -25.29243216311327913, 4.249687596552191415 ) ) ;
#2833=CARTESIAN_POINT ( 'NONE',  ( -30.57951140250705180, -25.14081846633245831, 7.291654623549840508 ) ) ;
#2834=CARTESIAN_POINT ( 'NONE',  ( -9.542874777335924819, 17.09510996321218101, 11.49999999999998934 ) ) ;
#2835=B_SPLINE_SURFACE_WITH_KNOTS ( 'NONE', 3, 3, ( 
 ( #94244, #24727, #2414, #62826 ),
 ( #55208, #79523, #49592, #10012 ),
 ( #86137, #95751, #56209, #25742 ),
 ( #57215, #11017, #16613, #71931 ),
 ( #72429, #47591, #55710, #33343 ),
 ( #64335, #10510, #64841, #48090 ),
 ( #25232, #78508, #88148, #24235 ),
 ( #18618, #1414, #9012, #80525 ),
 ( #9513, #41985, #39963, #56712 ),
 ( #87137, #40472, #79015, #87646 ) ),
 .UNSPECIFIED., .F., .F., .F.,
 ( 4, 3, 3, 4 ),
 ( 4, 4 ),
 ( 0.0004766839783845154836, 0.1491231665100183901, 0.2234464077758353262, 0.2977696490416522623 ),
 ( 0.04949997504963826039, 0.05054219714328903046 ),
 .UNSPECIFIED. ) ;
#2836=EDGE_CURVE ( 'NONE', #86491, #14136, #76058, .T. ) ;
#2839=CARTESIAN_POINT ( 'NONE',  ( -2.508422780830330989, 21.39056295969660582, 11.49999999999998934 ) ) ;
#2841=CARTESIAN_POINT ( 'NONE',  ( -75.52287095715004739, -25.00182538069145366, 7.747789668545101094 ) ) ;
#2842=ADVANCED_FACE ( 'NONE', ( #2497 ), #93560, .T. ) ;
#2844=CARTESIAN_POINT ( 'NONE',  ( -101.6526051508143382, -25.23550958530647748, 3.607042638994091277 ) ) ;
#2845=CARTESIAN_POINT ( 'NONE',  ( -77.62287095715004170, -23.96177878511308634, 10.65340807706329862 ) ) ;
#2846=CARTESIAN_POINT ( 'NONE',  ( 14.22603995551189371, 18.00578905361294346, -1.500000000000002220 ) ) ;
#2848=CARTESIAN_POINT ( 'NONE',  ( -84.92287095715008149, -23.47596703998600631, 11.44779298504227860 ) ) ;
#2849=CARTESIAN_POINT ( 'NONE',  ( -49.64567008890409028, -23.96119346886879953, -0.6495511937832114668 ) ) ;
#2850=CARTESIAN_POINT ( 'NONE',  ( -2.827821146493835425, 19.88259668395040691, 11.49999999999999645 ) ) ;
#2851=LINE ( 'NONE', #73843, #98071 ) ;
#2854=CARTESIAN_POINT ( 'NONE',  ( -82.62287095715005592, -24.65952944569304606, 1.056160979905699016 ) ) ;
#2856=EDGE_CURVE ( 'NONE', #64065, #73483, #94208, .T. ) ;
#2857=CARTESIAN_POINT ( 'NONE',  ( -126.5228709571500616, -23.48786465467241769, 11.44779295918253581 ) ) ;
#2858=CARTESIAN_POINT ( 'NONE',  ( 16.83370257367741019, -10.51912618480096206, -1.500000000000002220 ) ) ;
#2860=CARTESIAN_POINT ( 'NONE',  ( 17.62393913918218402, -8.800128315780904487, -1.500000000000002220 ) ) ;
#2865=CARTESIAN_POINT ( 'NONE',  ( -60.52287095715006160, -23.47596703998600631, 11.44779298504228926 ) ) ;
#2866=CARTESIAN_POINT ( 'NONE',  ( -39.04496629636555127, -25.28398045664843252, 4.275496105309666284 ) ) ;
#2867=CARTESIAN_POINT ( 'NONE',  ( 20.50092990308456464, -2.467789585553555654, 11.49999999999999645 ) ) ;
#2869=VECTOR ( 'NONE', #84348, 1000.000000000000114 ) ;
#2870=CARTESIAN_POINT ( 'NONE',  ( -128.5228709571500758, -23.48786465467242479, 11.44779295918253581 ) ) ;
#2871=CARTESIAN_POINT ( 'NONE',  ( -20.69567741759225399, -9.018594580484563750, 11.49999999999999645 ) ) ;
#2872=VERTEX_POINT ( 'NONE', #18214 ) ;
#2873=CARTESIAN_POINT ( 'NONE',  ( -69.56233234027952506, -25.12219073830083005, 6.775360582497007123 ) ) ;
#2874=CARTESIAN_POINT ( 'NONE',  ( -51.28856610397944849, -25.28231816955815603, 4.101867242166210126 ) ) ;
#2875=CARTESIAN_POINT ( 'NONE',  ( -64.52287095715004739, -24.34917612406836795, 0.1852690917426522976 ) ) ;
#2880=EDGE_CURVE ( 'NONE', #91650, #19525, #69954, .T. ) ;
#2881=ORIENTED_EDGE ( 'NONE', *, *, #37206, .F. ) ;
#2882=CARTESIAN_POINT ( 'NONE',  ( 21.72910700495702230, 7.846448622349001312, 11.49999999999999645 ) ) ;
#2883=CARTESIAN_POINT ( 'NONE',  ( 2.723195454624489642, 22.67993996152103620, 11.49999999999998934 ) ) ;
#2885=CARTESIAN_POINT ( 'NONE',  ( -106.6228709571501270, -23.96177878511308634, 10.65340807706329507 ) ) ;
#2886=CARTESIAN_POINT ( 'NONE',  ( -63.64183645978062032, -23.96169478059713143, 10.65365249895718236 ) ) ;
#2887=CARTESIAN_POINT ( 'NONE',  ( 16.76845895467136671, -15.01613412638008782, 11.49999999999999645 ) ) ;
#2889=CARTESIAN_POINT ( 'NONE',  ( -43.53993766296616030, -24.34968618360933235, 0.1864209137778850833 ) ) ;
#2890=CARTESIAN_POINT ( 'NONE',  ( -21.79611004543898289, 2.820803583321412678, 11.49999999999998934 ) ) ;
#2892=CARTESIAN_POINT ( 'NONE',  ( -111.5588656375797427, -23.48783264082477018, -1.443836473390086805 ) ) ;
#2893=CARTESIAN_POINT ( 'NONE',  ( -29.24573430514233507, -25.21724468935045138, 5.187748752069927249 ) ) ;
#2894=ORIENTED_EDGE ( 'NONE', *, *, #63272, .T. ) ;
#2895=CARTESIAN_POINT ( 'NONE',  ( -48.54083561204919306, -24.35071581493543036, 9.817618358456027039 ) ) ;
#2899=CARTESIAN_POINT ( 'NONE',  ( -68.92287095715006728, -23.47596703998600631, 11.44779298504227683 ) ) ;
#2900=CARTESIAN_POINT ( 'NONE',  ( -1.317410511717131971, -20.46822056820986546, 11.49999999999998934 ) ) ;
#2901=ORIENTED_EDGE ( 'NONE', *, *, #47493, .T. ) ;
#2903=EDGE_LOOP ( 'NONE', ( #54698, #71332, #28234, #8202, #30585, #82277, #21813, #24449, #14643 ) ) ;
#2904=CARTESIAN_POINT ( 'NONE',  ( -81.45489302840726964, -25.23432015487805558, 6.407480964600187789 ) ) ;
#2905=CARTESIAN_POINT ( 'NONE',  ( 19.36532470938277228, 12.59445105952145738, 11.49999999999998934 ) ) ;
#2907=CARTESIAN_POINT ( 'NONE',  ( 5.487062353440709472, 19.58251264919930534, -1.500000000000002220 ) ) ;
#2909=ORIENTED_EDGE ( 'NONE', *, *, #47982, .F. ) ;
#2911=CARTESIAN_POINT ( 'NONE',  ( -87.62287095715004170, -23.48783264082478794, -1.443836473390063269 ) ) ;
#2912=CARTESIAN_POINT ( 'NONE',  ( -51.50153678516716127, -25.20718309714190042, 3.380703470003659117 ) ) ;
#2913=CARTESIAN_POINT ( 'NONE',  ( -70.35895856474229504, -29.50249453571665725, 5.313164501615338153 ) ) ;
#2914=CARTESIAN_POINT ( 'NONE',  ( -66.52287095715006160, -24.64965694238407323, 8.947790433994200043 ) ) ;
#2916=CARTESIAN_POINT ( 'NONE',  ( -28.57654128002459260, -24.76880929330465975, 2.620674272415148831 ) ) ;
#2917=CARTESIAN_POINT ( 'NONE',  ( -93.52287095715006160, -23.47596703998600631, 11.44779298504228393 ) ) ;
#2919=CARTESIAN_POINT ( 'NONE',  ( -20.13249939377427111, -5.111880259578561514, -1.500000000000002220 ) ) ;
#2922=FACE_OUTER_BOUND ( 'NONE', #84486, .T. ) ;
#2923=ORIENTED_EDGE ( 'NONE', *, *, #52677, .T. ) ;
#2924=B_SPLINE_SURFACE_WITH_KNOTS ( 'NONE', 3, 3, ( 
 ( #34938, #4500, #89227, #19696 ),
 ( #35445, #58776, #48686, #60786 ),
 ( #52658, #82604, #35934, #68387 ),
 ( #12593, #43556, #37436, #82111 ),
 ( #44550, #91702, #98821, #36430 ),
 ( #14080, #74492, #51668, #51164 ),
 ( #14584, #5978, #37930, #59788 ),
 ( #5482, #99802, #29813, #60288 ),
 ( #20697, #28320, #4986, #61287 ),
 ( #28823, #66904, #22186, #97825 ) ),
 .UNSPECIFIED., .F., .F., .F.,
 ( 4, 3, 3, 4 ),
 ( 4, 4 ),
 ( 0.0004766839783818627120, 0.1491231665100170856, 0.2234464077758346878, 0.2977696490416523178 ),
 ( 0.1995180942284267289, 0.2006497111947407042 ),
 .UNSPECIFIED. ) ;
#2927=VERTEX_POINT ( 'NONE', #74490 ) ;
#2929=CARTESIAN_POINT ( 'NONE',  ( -29.62287095715004881, -23.39678932012542845, -1.443836140311830940 ) ) ;
#2930=CARTESIAN_POINT ( 'NONE',  ( -31.23108742109252134, -23.47593901973090169, -1.443836447538998424 ) ) ;
#2931=CARTESIAN_POINT ( 'NONE',  ( 21.13397978930849064, -6.478279476769641221, 11.49999999999999645 ) ) ;
#2932=ORIENTED_EDGE ( 'NONE', *, *, #56986, .F. ) ;
#2933=FACE_OUTER_BOUND ( 'NONE', #20590, .T. ) ;
#2934=CARTESIAN_POINT ( 'NONE',  ( -14.16962031475959272, 17.58799634409329471, 11.49999999999998934 ) ) ;
#2936=B_SPLINE_CURVE_WITH_KNOTS ( 'NONE', 3,
 ( #17819, #79205, #73117, #65523, #3605, #65026 ),
 .UNSPECIFIED., .F., .F.,
 ( 4, 2, 4 ),
 ( 6.391158118964604309E-06, 0.001387004593080786580, 0.002767618028042608501 ),
 .UNSPECIFIED. ) ;
#2937=CARTESIAN_POINT ( 'NONE',  ( -75.62287095715004170, -29.50249982740957577, 7.747779886224967605 ) ) ;
#2940=CARTESIAN_POINT ( 'NONE',  ( -93.52287095715006160, -23.47593901973090524, -1.443836447538996648 ) ) ;
#2944=CARTESIAN_POINT ( 'NONE',  ( -20.81765089029956783, 3.879123387127271005, 11.49999999999998934 ) ) ;
#2948=CARTESIAN_POINT ( 'NONE',  ( -20.66209241242137296, -8.185968977665980972, -1.500000000000002220 ) ) ;
#2953=CARTESIAN_POINT ( 'NONE',  ( -48.52287095715006160, -24.65952944569304606, 1.056160979905693686 ) ) ;
#2954=CARTESIAN_POINT ( 'NONE',  ( -18.23339674026497903, -6.527145932826366348, 11.49999999999999645 ) ) ;
#2955=CARTESIAN_POINT ( 'NONE',  ( -36.56104652793175802, -23.73791477778911130, 11.05961554403171121 ) ) ;
#2957=CARTESIAN_POINT ( 'NONE',  ( -4.154358412494840280, 19.03220294597612039, 11.49999999999998934 ) ) ;
#2959=CARTESIAN_POINT ( 'NONE',  ( 17.37860173834871347, 12.56526366372364301, 11.49999999999998934 ) ) ;
#2962=EDGE_CURVE ( 'NONE', #38599, #77757, #3484, .T. ) ;
#2963=CARTESIAN_POINT ( 'NONE',  ( -66.62287095715005592, -29.50250243563736774, 8.947779886222143375 ) ) ;
#2965=CARTESIAN_POINT ( 'NONE',  ( 16.48639501038195121, -15.69157857782056276, -1.500000000000002220 ) ) ;
#2967=CARTESIAN_POINT ( 'NONE',  ( -106.5112337399359035, -24.66019654487200441, 8.947790411086108620 ) ) ;
#2968=CARTESIAN_POINT ( 'NONE',  ( -101.5228709571500900, -24.66019654487200441, 8.947790411086119278 ) ) ;
#2969=CARTESIAN_POINT ( 'NONE',  ( 14.81759351585047391, 13.34335055255382052, 11.49999999999999645 ) ) ;
#2970=CARTESIAN_POINT ( 'NONE',  ( -78.55620429048339304, -24.64898659630528854, 1.056161002820828143 ) ) ;
#2971=B_SPLINE_CURVE_WITH_KNOTS ( 'NONE', 3,
 ( #23269, #78554, #38511, #92294 ),
 .UNSPECIFIED., .F., .F.,
 ( 4, 4 ),
 ( 0.000000000000000000, 1.000000000000000000 ),
 .UNSPECIFIED. ) ;
#2973=CARTESIAN_POINT ( 'NONE',  ( -56.92287095715008149, -23.47596703998600276, 11.44779298504227860 ) ) ;
#2975=ADVANCED_FACE ( 'NONE', ( #50665 ), #29312, .T. ) ;
#2976=PLANE ( 'NONE',  #5579 ) ;
#2977=CARTESIAN_POINT ( 'NONE',  ( -77.52287095715009002, -24.34917612406836795, 0.1852690917426540462 ) ) ;
#2978=B_SPLINE_CURVE_WITH_KNOTS ( 'NONE', 3,
 ( #35766, #52486, #83416, #13903 ),
 .UNSPECIFIED., .F., .F.,
 ( 4, 4 ),
 ( 0.4208004833249490706, 0.4298069145970646598 ),
 .UNSPECIFIED. ) ;
#2979=CARTESIAN_POINT ( 'NONE',  ( -21.46818342838279392, -2.986162219498790904, 11.49999999999998934 ) ) ;
#2980=CARTESIAN_POINT ( 'NONE',  ( -51.93149462243455616, -25.25905089634592571, 6.174051128686508072 ) ) ;
#2981=CARTESIAN_POINT ( 'NONE',  ( 13.74000504945409418, 13.82049530813991467, -1.500000000000002220 ) ) ;
#2982=CARTESIAN_POINT ( 'NONE',  ( -49.52287095715006160, -23.48783264082477018, -1.443836473390095465 ) ) ;
#2985=CARTESIAN_POINT ( 'NONE',  ( -69.62287095715009855, -23.95044443724992078, 10.65354141964650125 ) ) ;
#2986=CARTESIAN_POINT ( 'NONE',  ( 10.07161678670223637, 17.78519941539584792, 11.49999999999999645 ) ) ;
#2987=CARTESIAN_POINT ( 'NONE',  ( -128.5228709571500474, -23.48783264083417066, -1.443836473375472274 ) ) ;
#2988=B_SPLINE_CURVE_WITH_KNOTS ( 'NONE', 3,
 ( #53597, #22113, #14508, #45483 ),
 .UNSPECIFIED., .F., .F.,
 ( 4, 4 ),
 ( 0.000000000000000000, 0.0001000000000000167422 ),
 .UNSPECIFIED. ) ;
#2989=DIRECTION ( 'NONE',  ( 0.06474050504609950296, -0.8381167135261472501, -0.5416355246053439210 ) ) ;
#2991=CARTESIAN_POINT ( 'NONE',  ( -52.62287095715004170, -23.47596703998600276, 11.44779298504227505 ) ) ;
#2992=CARTESIAN_POINT ( 'NONE',  ( -40.52287095715006870, -23.48786465467241058, 11.44779295918255180 ) ) ;
#2993=CARTESIAN_POINT ( 'NONE',  ( -39.06913928595307084, -25.27985329021985805, 4.503859356828002092 ) ) ;
#2994=CARTESIAN_POINT ( 'NONE',  ( -49.28110964179429487, -25.31439463334452000, 6.053971487819386432 ) ) ;
#2995=CARTESIAN_POINT ( 'NONE',  ( -109.6260488237147257, -24.34968618360934300, 0.1864209137778879144 ) ) ;
#2996=ORIENTED_EDGE ( 'NONE', *, *, #70286, .F. ) ;
#2997=CARTESIAN_POINT ( 'NONE',  ( -66.59743546961844629, -23.96169478059713143, 10.65365249895718058 ) ) ;
#2999=ADVANCED_FACE ( 'NONE', ( #81613 ), #82109, .F. ) ;
#3000=CARTESIAN_POINT ( 'NONE',  ( -21.75629724252761577, 7.406401271465676395, 11.49999999999999645 ) ) ;
#3001=CARTESIAN_POINT ( 'NONE',  ( 18.68554041145753786, -12.99315341008173519, 11.49999999999998934 ) ) ;
#3002=CARTESIAN_POINT ( 'NONE',  ( -110.5124691553814102, -24.73531770709095312, 8.716586749053508498 ) ) ;
#3004=CARTESIAN_POINT ( 'NONE',  ( -81.52287095715006160, -23.47596703998600631, 11.44779298504228571 ) ) ;
#3005=CARTESIAN_POINT ( 'NONE',  ( -74.52287095715007581, -23.48786465467241058, 11.44779295918254647 ) ) ;
#3006=DIRECTION ( 'NONE',  ( 1.000000000000000000, 3.773278334444166432E-23, 8.201307841325785021E-29 ) ) ;
#3007=CARTESIAN_POINT ( 'NONE',  ( -19.96805355746080934, -8.928269573510897672, -1.500000000000002220 ) ) ;
#3008=CARTESIAN_POINT ( 'NONE',  ( -69.49425340576027565, -24.66019654487199375, 8.947790411086119278 ) ) ;
#3010=CARTESIAN_POINT ( 'NONE',  ( -27.39359161974487122, -24.75620229959870500, 2.307003371749687837 ) ) ;
#3011=DIRECTION ( 'NONE',  ( -3.773278334444166432E-23, 1.000000000000000000, 0.000000000000000000 ) ) ;
#3012=CARTESIAN_POINT ( 'NONE',  ( -99.14000973721185517, -25.31200576846117656, 5.341016405764093200 ) ) ;
#3013=VERTEX_POINT ( 'NONE', #59272 ) ;
#3015=CARTESIAN_POINT ( 'NONE',  ( -17.38880980700008294, 10.71821138944157603, 11.49999999999998934 ) ) ;
#3016=ORIENTED_EDGE ( 'NONE', *, *, #24626, .T. ) ;
#3018=CARTESIAN_POINT ( 'NONE',  ( 22.51966570110743149, 4.691836548664650053, -1.500000000000002220 ) ) ;
#3019=CARTESIAN_POINT ( 'NONE',  ( -80.52287095715001897, -24.52232992886362339, 0.6492154411906039257 ) ) ;
#3021=CARTESIAN_POINT ( 'NONE',  ( -29.52287095715006160, -24.57685061924431835, 8.947790457046968626 ) ) ;
#3024=CARTESIAN_POINT ( 'NONE',  ( -117.5800378283677929, -25.21791271819481750, 6.461860001696705602 ) ) ;
#3025=VECTOR ( 'NONE', #94064, 1000.000000000000114 ) ;
#3026=CARTESIAN_POINT ( 'NONE',  ( 21.30238844577196389, 2.035401582669650544, 11.49999999999999645 ) ) ;
#3029=CARTESIAN_POINT ( 'NONE',  ( -19.97062832128981213, -9.750827054148329509, -1.500000000000002220 ) ) ;
#3030=CARTESIAN_POINT ( 'NONE',  ( -4.528870947376731237, 20.18191347215651987, -1.500000000000002220 ) ) ;
#3031=EDGE_CURVE ( 'NONE', #56230, #85117, #66392, .T. ) ;
#3032=ORIENTED_EDGE ( 'NONE', *, *, #94322, .T. ) ;
#3036=CARTESIAN_POINT ( 'NONE',  ( -83.62287095715005592, -24.64965695001468404, 8.947790433994182280 ) ) ;
#3039=CARTESIAN_POINT ( 'NONE',  ( 19.90007246472742608, 6.374896562862660154, -1.500000000000002220 ) ) ;
#3040=CARTESIAN_POINT ( 'NONE',  ( -21.72861685410901700, 2.547970858986955189, 11.49999999999999645 ) ) ;
#3042=DIRECTION ( 'NONE',  ( -3.773278334453079030E-23, 0.9999999999976377785, 2.173523156925979128E-06 ) ) ;
#3043=CARTESIAN_POINT ( 'NONE',  ( 16.80569330386292748, 14.95695114220347932, 11.49999999999998934 ) ) ;
#3045=EDGE_CURVE ( 'NONE', #27537, #59423, #30039, .T. ) ;
#3046=CARTESIAN_POINT ( 'NONE',  ( 2.438461900574103502, 20.79476225230834174, -1.500000000000002220 ) ) ;
#3047=FACE_OUTER_BOUND ( 'NONE', #33648, .T. ) ;
#3050=ORIENTED_EDGE ( 'NONE', *, *, #34766, .F. ) ;
#3051=EDGE_CURVE ( 'NONE', #8894, #9998, #21597, .T. ) ;
#3054=CARTESIAN_POINT ( 'NONE',  ( -52.59322633568044125, -24.15543982623907482, -0.2315651400026529916 ) ) ;
#3055=ORIENTED_EDGE ( 'NONE', *, *, #37873, .T. ) ;
#3056=CARTESIAN_POINT ( 'NONE',  ( 9.091334071971768793, -19.38302982324925239, -1.500000000000002220 ) ) ;
#3057=ORIENTED_EDGE ( 'NONE', *, *, #15059, .F. ) ;
#3058=CARTESIAN_POINT ( 'NONE',  ( -59.52287095715006160, -24.65952944569304961, 1.056160979905695463 ) ) ;
#3059=CARTESIAN_POINT ( 'NONE',  ( -1.999300432013352058, 20.99099883833691749, -1.500000000000002220 ) ) ;
#3064=CARTESIAN_POINT ( 'NONE',  ( -50.59276831212685011, -24.40133493613049964, 9.663955038902802386 ) ) ;
#3065=CARTESIAN_POINT ( 'NONE',  ( -101.5550284192910482, -23.96119346886880663, -0.6495511937832049165 ) ) ;
#3066=CARTESIAN_POINT ( 'NONE',  ( -109.4123506053088306, -25.30719144561626877, 4.546003555234384486 ) ) ;
#3067=CARTESIAN_POINT ( 'NONE',  ( 21.39010012190943755, 5.354582491813655309, -1.500000000000002220 ) ) ;
#3068=ORIENTED_EDGE ( 'NONE', *, *, #45751, .T. ) ;
#3069=CARTESIAN_POINT ( 'NONE',  ( -65.58632257377641395, -24.63419186844610920, 9.035850630976922204 ) ) ;
#3070=EDGE_CURVE ( 'NONE', #11582, #5913, #25199, .T. ) ;
#3072=CARTESIAN_POINT ( 'NONE',  ( -63.52287095715004739, -23.47593901973090169, -1.443836447538996870 ) ) ;
#3073=VECTOR ( 'NONE', #23590, 1000.000000000000114 ) ;
#3074=CARTESIAN_POINT ( 'NONE',  ( -29.83767755215908579, -25.25218218361323963, 3.798368663089754182 ) ) ;
#3075=LINE ( 'NONE', #44500, #24622 ) ;
#3076=VECTOR ( 'NONE', #82099, 1000.000000000000114 ) ;
#3077=CARTESIAN_POINT ( 'NONE',  ( -57.62287095715004881, -24.64965695001468404, 8.947790433994185832 ) ) ;
#3078=CARTESIAN_POINT ( 'NONE',  ( -16.05942832139214360, -14.02155611864158402, -1.500000000000002220 ) ) ;
#3080=LINE ( 'NONE', #71587, #43068 ) ;
#3081=EDGE_CURVE ( 'NONE', #59423, #22424, #61519, .T. ) ;
#3083=CARTESIAN_POINT ( 'NONE',  ( -85.52287095715006160, -23.48783264082476663, -1.443836473390089470 ) ) ;
#3084=CARTESIAN_POINT ( 'NONE',  ( -5.352388609804938469, -21.92410630658433845, -1.500000000000002220 ) ) ;
#3085=B_SPLINE_CURVE_WITH_KNOTS ( 'NONE', 3,
 ( #61304, #53690, #92230, #53189, #14605, #5500 ),
 .UNSPECIFIED., .F., .F.,
 ( 4, 2, 4 ),
 ( 0.000000000000000000, 0.001380764517854767568, 0.002761529035709535135 ),
 .UNSPECIFIED. ) ;
#3086=EDGE_CURVE ( 'NONE', #88166, #85265, #948, .T. ) ;
#3087=PLANE ( 'NONE',  #91147 ) ;
#3088=VERTEX_POINT ( 'NONE', #39430 ) ;
#3091=CARTESIAN_POINT ( 'NONE',  ( -2.117704968268854682, 19.61795684621070990, 11.49999999999999645 ) ) ;
#3094=CARTESIAN_POINT ( 'NONE',  ( -40.52287095715005449, -23.48783264082476308, -1.443836473390097908 ) ) ;
#3095=B_SPLINE_CURVE_WITH_KNOTS ( 'NONE', 3,
 ( #69867, #78963, #31297, #85083, #32300, #61768 ),
 .UNSPECIFIED., .F., .F.,
 ( 4, 2, 4 ),
 ( 1.570755371634033063E-05, 0.001396183895866086886, 0.002776660238015833410 ),
 .UNSPECIFIED. ) ;
#3096=ORIENTED_EDGE ( 'NONE', *, *, #26536, .F. ) ;
#3097=EDGE_CURVE ( 'NONE', #53939, #31747, #5793, .T. ) ;
#3099=DIRECTION ( 'NONE',  ( -3.773278334453080206E-23, 0.9999999999976377785, 2.173523156925979975E-06 ) ) ;
#3100=CARTESIAN_POINT ( 'NONE',  ( -105.5228709571500616, -24.15516710230294706, 10.28746687063725496 ) ) ;
#3101=CARTESIAN_POINT ( 'NONE',  ( -21.33164055427280914, -3.227942221655450972, 11.49999999999998934 ) ) ;
#3102=FACE_OUTER_BOUND ( 'NONE', #78911, .T. ) ;
#3103=CARTESIAN_POINT ( 'NONE',  ( -76.55620429048340725, -24.66019654487199375, 8.947790411086128159 ) ) ;
#3106=PLANE ( 'NONE',  #81504 ) ;
#3107=CARTESIAN_POINT ( 'NONE',  ( -19.69265041987409859, 1.759638296948408787, 11.49999999999998934 ) ) ;
#3109=CARTESIAN_POINT ( 'NONE',  ( -19.75413285895528404, 4.560271753130525241, 11.49999999999999645 ) ) ;
#3111=VECTOR ( 'NONE', #24656, 1000.000000000000114 ) ;
#3113=CARTESIAN_POINT ( 'NONE',  ( -52.52287095715006870, -24.65952944569303895, 1.056160979905693686 ) ) ;
#3114=CARTESIAN_POINT ( 'NONE',  ( -99.54853273079524456, -25.27620648591849317, 4.157275027402507206 ) ) ;
#3115=CARTESIAN_POINT ( 'NONE',  ( -59.52287095715006160, -23.48786465467241769, 11.44779295918254824 ) ) ;
#3116=CARTESIAN_POINT ( 'NONE',  ( -31.52287095715006160, -23.48786465467240347, 11.44779295918255357 ) ) ;
#3119=CARTESIAN_POINT ( 'NONE',  ( 18.22975119132022215, -8.346483668847822557, 11.49999999999998934 ) ) ;
#3121=VERTEX_POINT ( 'NONE', #85594 ) ;
#3122=EDGE_CURVE ( 'NONE', #27644, #75868, #55405, .T. ) ;
#3123=CARTESIAN_POINT ( 'NONE',  ( -58.58953762381672448, -24.66019654487199375, 8.947790411086138818 ) ) ;
#3124=CARTESIAN_POINT ( 'NONE',  ( -35.47582077153254687, -24.73486907724917572, 1.287355809206972346 ) ) ;
#3125=CARTESIAN_POINT ( 'NONE',  ( -79.60960783475657365, -25.30268815552712525, 5.271914168462072503 ) ) ;
#3126=CARTESIAN_POINT ( 'NONE',  ( -60.52287095715006160, -29.50247984919015209, -1.443849546365056913 ) ) ;
#3127=CARTESIAN_POINT ( 'NONE',  ( -100.8386611319390340, -25.11990008798473539, 2.885623019206728479 ) ) ;
#3128=EDGE_CURVE ( 'NONE', #56669, #59957, #73555, .T. ) ;
#3129=CARTESIAN_POINT ( 'NONE',  ( -118.5228709571500758, -23.47593901973090524, -1.443836447538996204 ) ) ;
#3130=ORIENTED_EDGE ( 'NONE', *, *, #43922, .F. ) ;
#3133=CARTESIAN_POINT ( 'NONE',  ( -12.25758032491116367, 16.21837406056298292, -1.500000000000002220 ) ) ;
#3134=ORIENTED_EDGE ( 'NONE', *, *, #1202, .F. ) ;
#3136=CARTESIAN_POINT ( 'NONE',  ( -122.5228709571501327, -23.96127896941632329, -0.6493128931037981388 ) ) ;
#3138=VECTOR ( 'NONE', #67185, 1000.000000000000114 ) ;
#3139=CARTESIAN_POINT ( 'NONE',  ( -59.63219212808159853, -24.35071581493543746, 9.817618358456035921 ) ) ;
#3140=CARTESIAN_POINT ( 'NONE',  ( -50.36234373730416536, -25.12215419459477417, 7.100827092886333958 ) ) ;
#3142=CARTESIAN_POINT ( 'NONE',  ( -30.47287095715008221, -25.15028201304190603, 6.970007236040878240 ) ) ;
#3143=CARTESIAN_POINT ( 'NONE',  ( 15.88363568188429653, -14.04911357082368006, 11.49999999999999645 ) ) ;
#3145=CARTESIAN_POINT ( 'NONE',  ( -14.81638660137672225, 16.44347145309322045, -1.500000000000002220 ) ) ;
#3146=CARTESIAN_POINT ( 'NONE',  ( -10.57813111170615983, 17.65445453266677234, 11.49999999999998934 ) ) ;
#3149=CARTESIAN_POINT ( 'NONE',  ( -94.52287095715010423, -23.96177878511309345, 10.65340807706329862 ) ) ;
#3151=CARTESIAN_POINT ( 'NONE',  ( -54.62367899608845789, -24.65952944569304606, 1.056160979905696573 ) ) ;
#3152=CARTESIAN_POINT ( 'NONE',  ( -49.62287095715005592, -23.47593901973091235, -1.443836447539009749 ) ) ;
#3155=ORIENTED_EDGE ( 'NONE', *, *, #35938, .T. ) ;
#3156=CARTESIAN_POINT ( 'NONE',  ( -116.6228709571500559, -24.64965695001469115, 8.947790433994175174 ) ) ;
#3159=CARTESIAN_POINT ( 'NONE',  ( 15.29587703590233971, -13.95322596517325664, -1.500000000000002220 ) ) ;
#3160=CARTESIAN_POINT ( 'NONE',  ( 19.28387207504633949, -9.851753786812027514, 11.49999999999999645 ) ) ;
#3161=ORIENTED_EDGE ( 'NONE', *, *, #88054, .F. ) ;
#3162=EDGE_CURVE ( 'NONE', #58462, #54139, #50546, .T. ) ;
#3163=CARTESIAN_POINT ( 'NONE',  ( -98.89858548345738143, -25.26741689086502518, 5.967726646190992135 ) ) ;
#3164=CARTESIAN_POINT ( 'NONE',  ( -109.5562042904833646, -23.48786465467241769, 11.44779295918253581 ) ) ;
#3165=CARTESIAN_POINT ( 'NONE',  ( -12.73782554413503654, -18.45060914899308457, -1.500000000000002220 ) ) ;
#3170=ORIENTED_EDGE ( 'NONE', *, *, #13788, .T. ) ;
#3173=ADVANCED_FACE ( 'NONE', ( #47051 ), #55172, .F. ) ;
#3174=ORIENTED_EDGE ( 'NONE', *, *, #35349, .F. ) ;
#3175=ORIENTED_EDGE ( 'NONE', *, *, #68361, .F. ) ;
#3178=CARTESIAN_POINT ( 'NONE',  ( -100.9228709571500815, -23.47596703998600631, 11.44779298504227860 ) ) ;
#3179=CARTESIAN_POINT ( 'NONE',  ( 7.993063233546146229, -19.64520799392144568, -1.500000000000002220 ) ) ;
#3181=CARTESIAN_POINT ( 'NONE',  ( -88.64270303220058622, -23.48783264082477018, -1.443836473390093467 ) ) ;
#3182=CARTESIAN_POINT ( 'NONE',  ( -1.743439162979827595, 21.76861016152796324, -1.500000000000002220 ) ) ;
#3183=CARTESIAN_POINT ( 'NONE',  ( -52.49583607988384415, -24.35071581493542681, 9.817618358456037697 ) ) ;
#3184=CARTESIAN_POINT ( 'NONE',  ( -119.4728709571500502, -29.48149383318413541, 5.000941581248042667 ) ) ;
#3186=CARTESIAN_POINT ( 'NONE',  ( 16.40513048700843513, 14.50174154637248591, -1.500000000000002220 ) ) ;
#3187=DIRECTION ( 'NONE',  ( -3.773278334453079030E-23, 0.9999999999976377785, 2.173523156925979128E-06 ) ) ;
#3188=ORIENTED_EDGE ( 'NONE', *, *, #27940, .F. ) ;
#3190=CARTESIAN_POINT ( 'NONE',  ( -85.49691046782774606, -24.92592662359561473, 8.075495903018000021 ) ) ;
#3192=ADVANCED_FACE ( 'NONE', ( #18092 ), #1239, .T. ) ;
#3195=CARTESIAN_POINT ( 'NONE',  ( -90.62287095715002749, -24.83602698348159876, 1.605859176311266845 ) ) ;
#3197=DIRECTION ( 'NONE',  ( 0.000000000000000000, 0.9999999999976377785, 2.173523156925979128E-06 ) ) ;
#3198=CARTESIAN_POINT ( 'NONE',  ( -82.62632419238170201, -24.51314013834315375, 0.6176544820404169522 ) ) ;
#3199=CARTESIAN_POINT ( 'NONE',  ( -18.66175431467001999, 10.11895122522205526, -1.500000000000002220 ) ) ;
#3201=CARTESIAN_POINT ( 'NONE',  ( -30.56674980027052513, -25.57033040079277697, 6.142048374048878046 ) ) ;
#3204=FACE_OUTER_BOUND ( 'NONE', #20709, .T. ) ;
#3205=CARTESIAN_POINT ( 'NONE',  ( -129.5228709571501042, -24.34917612406838572, 0.1852690917426648154 ) ) ;
#3206=CARTESIAN_POINT ( 'NONE',  ( -2.795030477444873540, 19.22867370847827573, -1.500000000000002220 ) ) ;
#3207=CARTESIAN_POINT ( 'NONE',  ( -45.62377143496699006, -25.00158670708910691, 2.256160236439225031 ) ) ;
#3209=CARTESIAN_POINT ( 'NONE',  ( 11.71876819965036809, 15.69520123712499249, 11.49999999999999645 ) ) ;
#3211=AXIS2_PLACEMENT_3D ( 'NONE', #39172, #55924, #86846 ) ;
#3212=CARTESIAN_POINT ( 'NONE',  ( -33.62287095715005592, -29.50250243563736774, 8.947779886222150481 ) ) ;
#3213=EDGE_LOOP ( 'NONE', ( #55601, #25717, #70925, #79240 ) ) ;
#3214=ADVANCED_FACE ( 'NONE', ( #33816 ), #67593, .T. ) ;
#3216=CARTESIAN_POINT ( 'NONE',  ( -75.62287095715004170, -24.52232992886363405, 0.6492154411906084777 ) ) ;
#3218=B_SPLINE_CURVE_WITH_KNOTS ( 'NONE', 3,
 ( #58428, #59924, #81244, #83236 ),
 .UNSPECIFIED., .F., .F.,
 ( 4, 4 ),
 ( 0.000000000000000000, 1.000000000000000000 ),
 .UNSPECIFIED. ) ;
#3220=EDGE_CURVE ( 'NONE', #71152, #10158, #81994, .T. ) ;
#3221=CARTESIAN_POINT ( 'NONE',  ( -81.79035934495350091, -25.24813800626475668, 6.685839573822437210 ) ) ;
#3222=CARTESIAN_POINT ( 'NONE',  ( 19.69511366699831001, -0.05742560045514189665, 11.49999999999998934 ) ) ;
#3223=EDGE_CURVE ( 'NONE', #91718, #55380, #77116, .T. ) ;
#3227=PLANE ( 'NONE',  #3494 ) ;
#3228=FACE_OUTER_BOUND ( 'NONE', #274, .T. ) ;
#3232=CARTESIAN_POINT ( 'NONE',  ( -125.5228709571500900, -24.52323809116986197, 9.355190652339425483 ) ) ;
#3233=CARTESIAN_POINT ( 'NONE',  ( -105.6228709571500133, -24.14406661707766588, 10.28769366152058318 ) ) ;
#3234=DIRECTION ( 'NONE',  ( -3.773278334453080206E-23, 0.9999999999976377785, 2.173523156925979975E-06 ) ) ;
#3235=CARTESIAN_POINT ( 'NONE',  ( -97.63250974841577090, -23.96169478059714208, 10.65365249895717703 ) ) ;
#3236=CARTESIAN_POINT ( 'NONE',  ( -102.6228709571500559, -24.64965695001469115, 8.947790433994178727 ) ) ;
#3239=CARTESIAN_POINT ( 'NONE',  ( 19.59856454566043382, -3.714209461170434157, 11.49999999999998934 ) ) ;
#3240=CARTESIAN_POINT ( 'NONE',  ( -101.1018588697504157, -25.22871456504708121, 3.550613621098617223 ) ) ;
#3241=CARTESIAN_POINT ( 'NONE',  ( -1.345660788846553935, -19.86331345790170033, -1.500000000000002220 ) ) ;
#3242=VERTEX_POINT ( 'NONE', #75360 ) ;
#3243=LINE ( 'NONE', #88963, #23243 ) ;
#3244=CARTESIAN_POINT ( 'NONE',  ( -50.47208811125949524, -25.13340551635397091, 7.100116733165068972 ) ) ;
#3247=CARTESIAN_POINT ( 'NONE',  ( 13.57807927624399902, 15.74560944506941951, 11.49999999999999645 ) ) ;
#3249=CARTESIAN_POINT ( 'NONE',  ( -51.24209892600672589, -25.23977856974979517, 3.738451043460532031 ) ) ;
#3250=CARTESIAN_POINT ( 'NONE',  ( 12.37853024107498534, -19.16169124346054176, 11.49999999999999645 ) ) ;
#3251=ORIENTED_EDGE ( 'NONE', *, *, #60230, .T. ) ;
#3252=PLANE ( 'NONE',  #869 ) ;
#3253=CARTESIAN_POINT ( 'NONE',  ( -91.52287095715006160, -23.47596703998600631, 11.44779298504228393 ) ) ;
#3254=ORIENTED_EDGE ( 'NONE', *, *, #44216, .F. ) ;
#3255=CARTESIAN_POINT ( 'NONE',  ( 19.74221769882431587, -4.499994434135383692, 11.49999999999998934 ) ) ;
#3256=B_SPLINE_CURVE_WITH_KNOTS ( 'NONE', 3,
 ( #12824, #29054, #98558, #21924, #37173, #5721 ),
 .UNSPECIFIED., .F., .F.,
 ( 4, 2, 4 ),
 ( 1.570755371634376281E-05, 0.001396183895866091223, 0.002776660238015838614 ),
 .UNSPECIFIED. ) ;
#3257=CARTESIAN_POINT ( 'NONE',  ( -106.5228709571500758, -23.48786465467242479, 11.44779295918253936 ) ) ;
#3261=CARTESIAN_POINT ( 'NONE',  ( -79.26571160490151158, -25.31578574338585952, 5.001522333041759083 ) ) ;
#3263=CARTESIAN_POINT ( 'NONE',  ( -19.61284664649099696, 3.773188449817356904, -1.500000000000002220 ) ) ;
#3264=CARTESIAN_POINT ( 'NONE',  ( 19.44712688777480736, 7.780496645421295376, 11.49999999999999645 ) ) ;
#3267=CARTESIAN_POINT ( 'NONE',  ( 6.148021820315829444, -21.18842874637755358, 11.49999999999998934 ) ) ;
#3268=AXIS2_PLACEMENT_3D ( 'NONE', #4889, #11992, #20101 ) ;
#3269=CARTESIAN_POINT ( 'NONE',  ( -46.92287095715006018, -23.47593901973090169, -1.443836447538997980 ) ) ;
#3272=CARTESIAN_POINT ( 'NONE',  ( -122.5228709571500616, -29.50250243563736774, 8.947779886222134493 ) ) ;
#3274=CARTESIAN_POINT ( 'NONE',  ( -31.62287095715005236, -23.48783264082477729, -1.443836473390074149 ) ) ;
#3275=EDGE_CURVE ( 'NONE', #84354, #40031, #28607, .T. ) ;
#3278=EDGE_CURVE ( 'NONE', #80847, #69272, #65793, .T. ) ;
#3279=ORIENTED_EDGE ( 'NONE', *, *, #43912, .T. ) ;
#3281=CARTESIAN_POINT ( 'NONE',  ( -84.92287095715006728, -23.47593901973090169, -1.443836447538996870 ) ) ;
#3282=CARTESIAN_POINT ( 'NONE',  ( -51.52287095715008292, -23.47593901973090169, -1.443836447538997092 ) ) ;
#3283=CARTESIAN_POINT ( 'NONE',  ( -17.91610926057384034, -10.00117247862695358, -1.500000000000002220 ) ) ;
#3285=ORIENTED_EDGE ( 'NONE', *, *, #40044, .F. ) ;
#3286=DIRECTION ( 'NONE',  ( -3.773278334453079030E-23, 0.9999999999976377785, 2.173523156925979128E-06 ) ) ;
#3287=VECTOR ( 'NONE', #92886, 1000.000000000000114 ) ;
#3290=CARTESIAN_POINT ( 'NONE',  ( -12.45998644600372884, -18.51849504856558681, 11.49999999999998934 ) ) ;
#3291=ADVANCED_FACE ( 'NONE', ( #97709 ), #3883, .T. ) ;
#3293=CARTESIAN_POINT ( 'NONE',  ( -0.1256113942619183910, -21.42386179076044073, -0.9709657327914303915 ) ) ;
#3294=CARTESIAN_POINT ( 'NONE',  ( -32.99388727629348494, -25.12026506542017046, 2.831122744435439209 ) ) ;
#3295=ORIENTED_EDGE ( 'NONE', *, *, #77382, .F. ) ;
#3298=FACE_OUTER_BOUND ( 'NONE', #96131, .T. ) ;
#3300=B_SPLINE_CURVE_WITH_KNOTS ( 'NONE', 3,
 ( #63380, #70974, #48142, #1464, #25285, #17676 ),
 .UNSPECIFIED., .F., .F.,
 ( 4, 2, 4 ),
 ( 6.384118678612496926E-06, 0.001386860460828376286, 0.002767336802978140158 ),
 .UNSPECIFIED. ) ;
#3301=CARTESIAN_POINT ( 'NONE',  ( 12.78316523911058944, -16.47895720935621711, -1.500000000000002220 ) ) ;
#3303=CARTESIAN_POINT ( 'NONE',  ( -40.07618229162368095, -25.11765537177068808, 2.873089416660186135 ) ) ;
#3305=ORIENTED_EDGE ( 'NONE', *, *, #42415, .F. ) ;
#3307=LINE ( 'NONE', #27121, #6581 ) ;
#3308=CARTESIAN_POINT ( 'NONE',  ( 20.75205275252385206, -3.532026382766447536, -1.500000000000002220 ) ) ;
#3309=VECTOR ( 'NONE', #55680, 1000.000000000000114 ) ;
#3311=LINE ( 'NONE', #59082, #12197 ) ;
#3312=CARTESIAN_POINT ( 'NONE',  ( -53.52287095715006160, -23.95044443724992789, 10.65354141964649415 ) ) ;
#3313=CARTESIAN_POINT ( 'NONE',  ( -120.5553384622658939, -24.15602025860899360, 10.28564288303534902 ) ) ;
#3314=FACE_OUTER_BOUND ( 'NONE', #86391, .T. ) ;
#3315=CARTESIAN_POINT ( 'NONE',  ( -83.62287095715005592, -23.47593901973091235, -1.443836447539004642 ) ) ;
#3316=CARTESIAN_POINT ( 'NONE',  ( 21.03555826204448209, -5.341079136732027166, -1.500000000000002220 ) ) ;
#3317=CARTESIAN_POINT ( 'NONE',  ( -81.04964064216432007, -25.24759771266412045, 6.946763360114873720 ) ) ;
#3318=CARTESIAN_POINT ( 'NONE',  ( 2.321567282091853812, -22.14299765706108403, 11.49999999999999645 ) ) ;
#3320=CARTESIAN_POINT ( 'NONE',  ( -51.50851365739161736, -25.31441895692774935, 5.995695726151790694 ) ) ;
#3323=CARTESIAN_POINT ( 'NONE',  ( -69.62287095715005592, -23.48786465467241058, 11.44779295918254824 ) ) ;
#3325=CARTESIAN_POINT ( 'NONE',  ( -76.62287095715009855, -24.50216790748098816, 0.6166512839513735855 ) ) ;
#3326=ORIENTED_EDGE ( 'NONE', *, *, #2145, .F. ) ;
#3327=EDGE_CURVE ( 'NONE', #74882, #1888, #73879, .T. ) ;
#3330=CARTESIAN_POINT ( 'NONE',  ( -107.5228709571500758, -24.65952944569304961, 1.056160979905704123 ) ) ;
#3331=CARTESIAN_POINT ( 'NONE',  ( -126.5228709571500616, -24.64965694238408034, 8.947790433994189385 ) ) ;
#3332=ORIENTED_EDGE ( 'NONE', *, *, #70416, .F. ) ;
#3334=CARTESIAN_POINT ( 'NONE',  ( 15.48037617655995923, 16.25473645317415361, -1.500000000000002220 ) ) ;
#3335=VERTEX_POINT ( 'NONE', #59160 ) ;
#3337=CARTESIAN_POINT ( 'NONE',  ( -101.5888304102239630, -24.35071581493543746, 9.817618358456027039 ) ) ;
#3340=CARTESIAN_POINT ( 'NONE',  ( -63.93323764602512682, -24.26827793580486059, 9.960784317162946877 ) ) ;
#3342=CARTESIAN_POINT ( 'NONE',  ( 19.39309126630920588, -2.812899550206792831, 11.49999999999998934 ) ) ;
#3343=CARTESIAN_POINT ( 'NONE',  ( -59.55620429048337883, -24.65952944569304961, 1.056160979905694797 ) ) ;
#3345=CARTESIAN_POINT ( 'NONE',  ( -18.53595284743415661, 10.95218985133829825, -1.500000000000002220 ) ) ;
#3346=CARTESIAN_POINT ( 'NONE',  ( -60.62287095715004881, -23.48783264082478439, -1.443836473390068820 ) ) ;
#3347=CARTESIAN_POINT ( 'NONE',  ( -71.28784841027113828, -25.12218989441461048, 6.387103282270394367 ) ) ;
#3350=ADVANCED_FACE ( 'NONE', ( #28203 ), #89109, .F. ) ;
#3351=CARTESIAN_POINT ( 'NONE',  ( -77.62287095715007013, -23.48786465467241413, 11.44779295918254469 ) ) ;
#3352=CARTESIAN_POINT ( 'NONE',  ( -16.74478417649319084, -15.65585335247391896, -1.500000000000002220 ) ) ;
#3354=DIRECTION ( 'NONE',  ( 0.000000000000000000, -2.173523156925979552E-06, 0.9999999999976378895 ) ) ;
#3355=DIRECTION ( 'NONE',  ( 1.000000000000000000, 3.773278334444166432E-23, 8.201307841325785021E-29 ) ) ;
#3356=CARTESIAN_POINT ( 'NONE',  ( -16.07871291144651593, -12.00523380332558965, 11.49999999999999645 ) ) ;
#3357=CARTESIAN_POINT ( 'NONE',  ( -109.7637679387061809, -25.28814089820113153, 2.928686338884283202 ) ) ;
#3359=B_SPLINE_CURVE_WITH_KNOTS ( 'NONE', 3,
 ( #80227, #57414, #34563, #58895, #4615, #35562 ),
 .UNSPECIFIED., .F., .F.,
 ( 4, 2, 4 ),
 ( 1.570887131794333942E-05, 0.001396322306279761073, 0.002776935741241578874 ),
 .UNSPECIFIED. ) ;
#3361=CARTESIAN_POINT ( 'NONE',  ( -82.52287095715006160, -29.50248528299804818, 1.056150453629038477 ) ) ;
#3362=CARTESIAN_POINT ( 'NONE',  ( -96.22287095715006444, -23.47596703998600631, 11.44779298504227860 ) ) ;
#3363=CARTESIAN_POINT ( 'NONE',  ( -7.754168067426306266, 18.25094163199162622, -1.500000000000002220 ) ) ;
#3365=CARTESIAN_POINT ( 'NONE',  ( -14.27994306655487300, -13.59162091658854798, -1.500000000000002220 ) ) ;
#3366=CARTESIAN_POINT ( 'NONE',  ( -75.58953762381673869, -23.48786465467241058, 11.44779295918254647 ) ) ;
#3369=AXIS2_PLACEMENT_3D ( 'NONE', #15600, #24712, #77492 ) ;
#3370=CARTESIAN_POINT ( 'NONE',  ( -57.52287095715005449, -23.47596703998600631, 11.44779298504228926 ) ) ;
#3372=CARTESIAN_POINT ( 'NONE',  ( 18.07347782881280907, 9.871946371954690491, 11.49999999999999645 ) ) ;
#3373=CARTESIAN_POINT ( 'NONE',  ( -42.62287095715007013, -23.96127896941632685, -0.6493128931037909224 ) ) ;
#3375=CARTESIAN_POINT ( 'NONE',  ( -21.51096707683950626, -7.176001652309477841, 11.49999999999999645 ) ) ;
#3376=ORIENTED_EDGE ( 'NONE', *, *, #22735, .F. ) ;
#3377=CARTESIAN_POINT ( 'NONE',  ( -126.5562042904833930, -23.47593901973091235, -1.443836447538995760 ) ) ;
#3378=CARTESIAN_POINT ( 'NONE',  ( -50.60192890204033489, -25.31221690582124140, 4.716031646587921067 ) ) ;
#3379=CARTESIAN_POINT ( 'NONE',  ( -110.6228709571500559, -24.51254535404253687, 9.355368623467654743 ) ) ;
#3380=CARTESIAN_POINT ( 'NONE',  ( -56.52287095715009713, -23.96177878511308990, 10.65340807706330217 ) ) ;
#3381=ORIENTED_EDGE ( 'NONE', *, *, #54926, .T. ) ;
#3383=B_SPLINE_CURVE_WITH_KNOTS ( 'NONE', 3,
 ( #85212, #32431, #56290, #30925 ),
 .UNSPECIFIED., .F., .F.,
 ( 4, 4 ),
 ( 0.000000000000000000, 0.0001000000000000167422 ),
 .UNSPECIFIED. ) ;
#3384=CARTESIAN_POINT ( 'NONE',  ( -15.12447472116105729, 17.10960193589383849, -1.500000000000002220 ) ) ;
#3385=CARTESIAN_POINT ( 'NONE',  ( -100.5228709571500758, -23.47593901973090524, -1.443836447538996648 ) ) ;
#3388=CARTESIAN_POINT ( 'NONE',  ( -22.32441756149717094, -2.617931739244098388, 11.49999999999999645 ) ) ;
#3390=B_SPLINE_CURVE_WITH_KNOTS ( 'NONE', 3,
 ( #36995, #28885, #98887, #90787 ),
 .UNSPECIFIED., .F., .F.,
 ( 4, 4 ),
 ( 9.399644415434986408E-16, 2.036287925413292384E-05 ),
 .UNSPECIFIED. ) ;
#3391=CARTESIAN_POINT ( 'NONE',  ( -43.64074243423868182, -24.15543982623907127, -0.2315651400026568496 ) ) ;
#3392=CARTESIAN_POINT ( 'NONE',  ( 21.10488023177059347, -6.046698511884514460, -1.500000000000002220 ) ) ;
#3395=CARTESIAN_POINT ( 'NONE',  ( -70.16027724210108829, -25.03456847279097630, 7.555221055302367539 ) ) ;
#3396=ORIENTED_EDGE ( 'NONE', *, *, #24926, .F. ) ;
#3397=CARTESIAN_POINT ( 'NONE',  ( -92.62287095715005592, -29.50248528299804818, 1.056150453629040253 ) ) ;
#3399=ORIENTED_EDGE ( 'NONE', *, *, #68320, .T. ) ;
#3400=CARTESIAN_POINT ( 'NONE',  ( -54.62797921530123801, -24.51419770103157347, 9.386484678747176957 ) ) ;
#3401=EDGE_CURVE ( 'NONE', #87031, #642, #60169, .T. ) ;
#3402=CARTESIAN_POINT ( 'NONE',  ( 20.49162120248849561, -0.4999214236376636200, -1.500000000000002220 ) ) ;
#3403=VERTEX_POINT ( 'NONE', #81990 ) ;
#3404=ORIENTED_EDGE ( 'NONE', *, *, #17334, .F. ) ;
#3407=CARTESIAN_POINT ( 'NONE',  ( 8.286623624103266097E-13, -23.05000000000000426, 11.49999999999998934 ) ) ;
#3409=CARTESIAN_POINT ( 'NONE',  ( -12.25758032491116367, 16.21837406056298292, -1.500000000000002220 ) ) ;
#3410=EDGE_CURVE ( 'NONE', #57091, #76361, #87920, .T. ) ;
#3411=ORIENTED_EDGE ( 'NONE', *, *, #42967, .F. ) ;
#3413=CARTESIAN_POINT ( 'NONE',  ( -29.66017770924821306, -23.66242766326485736, 11.05961561336856569 ) ) ;
#3414=EDGE_CURVE ( 'NONE', #65188, #68864, #89603, .T. ) ;
#3415=CARTESIAN_POINT ( 'NONE',  ( -105.5894920141959687, -24.52300882791530157, 0.6510814631126371488 ) ) ;
#3416=CARTESIAN_POINT ( 'NONE',  ( -70.70237668956666255, -25.25855373138085014, 7.522646402401707455 ) ) ;
#3417=ORIENTED_EDGE ( 'NONE', *, *, #32360, .F. ) ;
#3418=CARTESIAN_POINT ( 'NONE',  ( -27.68651082257922980, -24.76880854176360813, 2.274903372879362617 ) ) ;
#3419=CARTESIAN_POINT ( 'NONE',  ( -99.52287095715011844, -23.48783264083466449, -1.443836473374706442 ) ) ;
#3420=EDGE_CURVE ( 'NONE', #57878, #62448, #50054, .T. ) ;
#3423=CARTESIAN_POINT ( 'NONE',  ( -2.730994233912177549, 20.60462238790213618, 11.49999999999998934 ) ) ;
#3426=CARTESIAN_POINT ( 'NONE',  ( -39.45233922144024064, -25.28612432382913511, 4.312181222606807474 ) ) ;
#3428=DIRECTION ( 'NONE',  ( -3.773278334453079618E-23, 0.9999999999976377785, 2.173523156925979975E-06 ) ) ;
#3430=ORIENTED_EDGE ( 'NONE', *, *, #44468, .F. ) ;
#3431=ORIENTED_EDGE ( 'NONE', *, *, #5842, .F. ) ;
#3432=DIRECTION ( 'NONE',  ( -3.773278334453079618E-23, 0.9999999999976377785, 2.173523156925979975E-06 ) ) ;
#3433=DIRECTION ( 'NONE',  ( 1.000000000000000000, 3.773278334444166432E-23, 8.201307841325785021E-29 ) ) ;
#3434=CARTESIAN_POINT ( 'NONE',  ( -71.30457154551152144, -25.24515236888725056, 6.209207408895393243 ) ) ;
#3435=CARTESIAN_POINT ( 'NONE',  ( -20.36895902721504825, -8.506870616244709637, 11.49999999999999645 ) ) ;
#3436=VERTEX_POINT ( 'NONE', #48301 ) ;
#3438=CARTESIAN_POINT ( 'NONE',  ( -19.18631400275845422, -11.98935526391121087, 11.49999999999998934 ) ) ;
#3446=VERTEX_POINT ( 'NONE', #29695 ) ;
#3447=CARTESIAN_POINT ( 'NONE',  ( 9.297385241821217505, 19.04214385377821017, -1.500000000000002220 ) ) ;
#3448=CARTESIAN_POINT ( 'NONE',  ( -78.97085663747836293, -25.03138025248980725, 6.301136368351477834 ) ) ;
#3450=CARTESIAN_POINT ( 'NONE',  ( -41.18130138025338738, -25.29969733389206965, 5.386376836069856289 ) ) ;
#3451=CARTESIAN_POINT ( 'NONE',  ( 17.16062296631688255, 14.07911611715085876, -1.500000000000002220 ) ) ;
#3452=CARTESIAN_POINT ( 'NONE',  ( -49.44333826525905806, -25.13941437307980920, 7.288210270445980576 ) ) ;
#3453=EDGE_LOOP ( 'NONE', ( #42380, #36140, #60518, #70811 ) ) ;
#3456=CARTESIAN_POINT ( 'NONE',  ( -40.80745846450592040, -25.11777459330632922, 2.873756378189262772 ) ) ;
#3458=CARTESIAN_POINT ( 'NONE',  ( 18.23270504744370868, -6.907985942191454676, 11.49999999999998934 ) ) ;
#3459=CARTESIAN_POINT ( 'NONE',  ( 21.40653236543258231, -1.377805879665675803, 11.49999999999998934 ) ) ;
#3460=CARTESIAN_POINT ( 'NONE',  ( -27.12458168156152638, -24.57999515849961369, 1.715463076443914936 ) ) ;
#3461=CARTESIAN_POINT ( 'NONE',  ( -107.5895376238167387, -23.48786465467241769, 11.44779295918253936 ) ) ;
#3462=DIRECTION ( 'NONE',  ( -1.000000000000000000, -3.773278334444166432E-23, -8.201307841325785021E-29 ) ) ;
#3463=EDGE_CURVE ( 'NONE', #3899, #39432, #29865, .T. ) ;
#3464=CARTESIAN_POINT ( 'NONE',  ( -12.29745307268338195, -19.16510367807413218, -1.500000000000002220 ) ) ;
#3466=CARTESIAN_POINT ( 'NONE',  ( -102.5955334420205105, -23.73766607897671932, -1.055555164236430477 ) ) ;
#3468=CARTESIAN_POINT ( 'NONE',  ( -12.53609265798794681, -15.47265773855268378, 11.49999999999999645 ) ) ;
#3469=CARTESIAN_POINT ( 'NONE',  ( -31.52287095715004028, -23.94994826722564696, -0.6494450866342755813 ) ) ;
#3470=CARTESIAN_POINT ( 'NONE',  ( -128.5228709571500474, -24.50321055353803601, 9.387540953477504502 ) ) ;
#3472=ORIENTED_EDGE ( 'NONE', *, *, #86762, .T. ) ;
#3473=CARTESIAN_POINT ( 'NONE',  ( -25.55988077703415939, -24.90308938919016768, 4.202771167367211902 ) ) ;
#3475=CARTESIAN_POINT ( 'NONE',  ( 8.489507321284875729, -19.98171680480944445, -1.500000000000002220 ) ) ;
#3476=CARTESIAN_POINT ( 'NONE',  ( -51.88092039732551086, -25.21678524435695223, 6.552750624006524305 ) ) ;
#3477=CARTESIAN_POINT ( 'NONE',  ( -6.365771329251782795, -18.49506561991874065, -1.500000000000002220 ) ) ;
#3479=ORIENTED_EDGE ( 'NONE', *, *, #82080, .F. ) ;
#3481=CARTESIAN_POINT ( 'NONE',  ( -60.62287095715003460, -24.83620972994591014, 8.398175272781363887 ) ) ;
#3482=CARTESIAN_POINT ( 'NONE',  ( -8.052747710315523832, 18.77774781879659116, 11.49999999999999645 ) ) ;
#3484=B_SPLINE_CURVE_WITH_KNOTS ( 'NONE', 3,
 ( #97823, #36927, #13579, #66902, #20695, #44547, #19693, #96830 ),
 .UNSPECIFIED., .F., .F.,
 ( 4, 2, 2, 4 ),
 ( -0.001240355328176650195, -0.0002398155169397891452, 0.0007607242942970719041, 0.002761803916770794003 ),
 .UNSPECIFIED. ) ;
#3485=AXIS2_PLACEMENT_3D ( 'NONE', #3361, #57639, #11944 ) ;
#3486=CARTESIAN_POINT ( 'NONE',  ( -89.52287095715011844, -23.94994826722565406, -0.6494450866342716955 ) ) ;
#3487=ORIENTED_EDGE ( 'NONE', *, *, #33526, .T. ) ;
#3488=CARTESIAN_POINT ( 'NONE',  ( -53.22287095715005023, -23.47596703998600276, 11.44779298504227860 ) ) ;
#3489=DIRECTION ( 'NONE',  ( -3.773278334444167608E-23, 1.000000000000000000, 0.000000000000000000 ) ) ;
#3490=CARTESIAN_POINT ( 'NONE',  ( -63.52287095715006160, -29.50250243563736774, 8.947779886222145151 ) ) ;
#3491=CARTESIAN_POINT ( 'NONE',  ( -56.52287095715005449, -23.47593901973090169, -1.443836447538996870 ) ) ;
#3493=CARTESIAN_POINT ( 'NONE',  ( -66.58005638815387783, -24.66019654487199375, 8.947790411086119278 ) ) ;
#3494=AXIS2_PLACEMENT_3D ( 'NONE', #9812, #35158, #18426 ) ;
#3495=CARTESIAN_POINT ( 'NONE',  ( -6.529369910325518944, -22.02198592821369516, 11.49999999999999645 ) ) ;
#3496=CARTESIAN_POINT ( 'NONE',  ( 5.860688371469950475, 21.97560254587667217, -1.500000000000002220 ) ) ;
#3498=CARTESIAN_POINT ( 'NONE',  ( -91.58953762381673869, -23.48786465467241769, 11.44779295918254114 ) ) ;
#3499=CARTESIAN_POINT ( 'NONE',  ( -90.50269887387773338, -24.73486907724917927, 1.287355809206966573 ) ) ;
#3503=CARTESIAN_POINT ( 'NONE',  ( 6.672210613628693388, 20.84999943921648935, -1.500000000000002220 ) ) ;
#3504=CARTESIAN_POINT ( 'NONE',  ( -74.52287095715009002, -23.94994826722564696, -0.6494450866342713624 ) ) ;
#3505=CARTESIAN_POINT ( 'NONE',  ( -48.91427541414667957, -25.28859040982994344, 5.814958163393877832 ) ) ;
#3507=CARTESIAN_POINT ( 'NONE',  ( -96.52287095715011844, -24.33927499327855770, 9.819080762295806508 ) ) ;
#3509=CARTESIAN_POINT ( 'NONE',  ( 8.094744887094867281, -18.73235182305680624, -1.500000000000002220 ) ) ;
#3511=EDGE_LOOP ( 'NONE', ( #41596, #12392, #54523, #87657 ) ) ;
#3513=CARTESIAN_POINT ( 'NONE',  ( -4.971178678486217528, -22.47594730032828281, 11.49999999999998934 ) ) ;
#3514=PLANE ( 'NONE',  #94019 ) ;
#3515=CARTESIAN_POINT ( 'NONE',  ( 16.68447708738676383, -11.30049470069299922, -1.500000000000002220 ) ) ;
#3519=CARTESIAN_POINT ( 'NONE',  ( -95.62462609076078479, -24.92564183028979841, 1.928384488918254425 ) ) ;
#3520=FACE_OUTER_BOUND ( 'NONE', #98848, .T. ) ;
#3521=CARTESIAN_POINT ( 'NONE',  ( 19.99361899508246765, -7.638522130635823082, 11.49999999999999645 ) ) ;
#3522=ORIENTED_EDGE ( 'NONE', *, *, #92533, .T. ) ;
#3526=CARTESIAN_POINT ( 'NONE',  ( -9.338385371603758145, -20.21602636099808237, 11.49999999999998934 ) ) ;
#3528=CARTESIAN_POINT ( 'NONE',  ( -9.011640028862021978, 18.61544202926687674, -1.500000000000002220 ) ) ;
#3531=B_SPLINE_CURVE_WITH_KNOTS ( 'NONE', 3,
 ( #77455, #87083, #63269, #62261, #17572, #7955 ),
 .UNSPECIFIED., .F., .F.,
 ( 4, 2, 4 ),
 ( 1.570755371633915156E-05, 0.001396183895866087103, 0.002776660238015835145 ),
 .UNSPECIFIED. ) ;
#3533=EDGE_LOOP ( 'NONE', ( #37244, #89735, #94262, #12625 ) ) ;
#3537=CARTESIAN_POINT ( 'NONE',  ( 19.40473180639871131, -7.901900427366274293, -1.500000000000002220 ) ) ;
#3538=ADVANCED_FACE ( 'NONE', ( #6855 ), #78712, .T. ) ;
#3539=CARTESIAN_POINT ( 'NONE',  ( -19.20277006422315225, 10.48866939257135833, 11.49999999999999645 ) ) ;
#3540=CARTESIAN_POINT ( 'NONE',  ( -26.92109862195654202, -24.77993744210030158, 7.359062092904308017 ) ) ;
#3541=CARTESIAN_POINT ( 'NONE',  ( 17.90692129536829924, 13.62026984716248101, -1.500000000000002220 ) ) ;
#3542=CARTESIAN_POINT ( 'NONE',  ( 7.003190781191628744, -19.75400906848480176, 11.49999999999998934 ) ) ;
#3543=CARTESIAN_POINT ( 'NONE',  ( -26.18848782724420232, -24.88148942182913004, 5.990951222462844505 ) ) ;
#3544=CARTESIAN_POINT ( 'NONE',  ( -108.8968792378191921, -25.06732983082694943, 7.447789526168955732 ) ) ;
#3545=CARTESIAN_POINT ( 'NONE',  ( -70.52287095715007581, -23.47596703998600631, 11.44779298504228748 ) ) ;
#3550=CARTESIAN_POINT ( 'NONE',  ( -52.56018645129599065, -23.73766607897671577, -1.055555164236436472 ) ) ;
#3552=CARTESIAN_POINT ( 'NONE',  ( -17.67684169981329845, 12.20363403927300183, -1.500000000000002220 ) ) ;
#3553=ORIENTED_EDGE ( 'NONE', *, *, #97201, .F. ) ;
#3554=DIRECTION ( 'NONE',  ( -1.000000000000000000, -3.773278334444166432E-23, -8.201307841325785021E-29 ) ) ;
#3555=CARTESIAN_POINT ( 'NONE',  ( 2.841100885065937387, 20.89556961663114265, 11.49999999999998934 ) ) ;
#3556=CARTESIAN_POINT ( 'NONE',  ( -30.53009340616916134, -23.47882956801885612, 11.44779287168131710 ) ) ;
#3559=B_SPLINE_CURVE_WITH_KNOTS ( 'NONE', 3,
 ( #48769, #65010, #71099, #95926 ),
 .UNSPECIFIED., .F., .F.,
 ( 4, 4 ),
 ( 2.775557561562891043E-17, 9.999999999998898659E-05 ),
 .UNSPECIFIED. ) ;
#3560=FACE_OUTER_BOUND ( 'NONE', #10417, .T. ) ;
#3561=CARTESIAN_POINT ( 'NONE',  ( -129.5900272792847829, -23.48786465467242124, 11.44779295918253936 ) ) ;
#3562=CARTESIAN_POINT ( 'NONE',  ( 20.57837473233041692, -7.934362236255416256, -1.500000000000002220 ) ) ;
#3564=CARTESIAN_POINT ( 'NONE',  ( -116.6251875513247853, -24.34968618360935366, 0.1864209137779019310 ) ) ;
#3568=ADVANCED_FACE ( 'NONE', ( #84973 ), #83793, .T. ) ;
#3569=CARTESIAN_POINT ( 'NONE',  ( -26.94934480766437090, -25.03522359940358655, 4.936952632524853612 ) ) ;
#3570=VECTOR ( 'NONE', #38406, 1000.000000000000114 ) ;
#3571=B_SPLINE_CURVE_WITH_KNOTS ( 'NONE', 3,
 ( #70608, #32045, #41171, #63016, #64033, #94947 ),
 .UNSPECIFIED., .F., .F.,
 ( 4, 2, 4 ),
 ( 0.000000000000000000, 0.001380764517853247299, 0.002761529035706494599 ),
 .UNSPECIFIED. ) ;
#3572=DIRECTION ( 'NONE',  ( 3.773278334444166432E-23, -1.000000000000000000, 0.000000000000000000 ) ) ;
#3575=CARTESIAN_POINT ( 'NONE',  ( 15.73328655151706101, -14.44092690703295467, -1.500000000000002220 ) ) ;
#3576=PLANE ( 'NONE',  #46616 ) ;
#3577=CARTESIAN_POINT ( 'NONE',  ( -52.55620429048339304, -23.48783264082477729, -1.443836473390070596 ) ) ;
#3578=ADVANCED_FACE ( 'NONE', ( #64049 ), #91078, .T. ) ;
#3580=CARTESIAN_POINT ( 'NONE',  ( -81.48149462243459595, -25.23679622552714363, 6.293943003980942308 ) ) ;
#3581=CARTESIAN_POINT ( 'NONE',  ( 14.59886444729927923, 17.24780449347180067, -1.500000000000002220 ) ) ;
#3583=ORIENTED_EDGE ( 'NONE', *, *, #76468, .F. ) ;
#3585=CARTESIAN_POINT ( 'NONE',  ( -79.63359157097742980, -24.15543982623907127, -0.2315651400026654261 ) ) ;
#3586=CARTESIAN_POINT ( 'NONE',  ( -9.637476322613308000, -17.25261889746210997, 11.49999999999999645 ) ) ;
#3587=CARTESIAN_POINT ( 'NONE',  ( -123.6228709571500559, -24.66019654487200086, 8.947790411086117501 ) ) ;
#3588=CARTESIAN_POINT ( 'NONE',  ( -67.51596563316087440, -23.73766607897670511, -1.055555164236457788 ) ) ;
#3590=CARTESIAN_POINT ( 'NONE',  ( -79.11611000704996854, -25.21083105912962097, 3.409327675794633361 ) ) ;
#3593=CARTESIAN_POINT ( 'NONE',  ( -21.62496174240652991, 0.2022338437372764308, 11.49999999999998934 ) ) ;
#3597=CARTESIAN_POINT ( 'NONE',  ( -80.93923948188344752, -25.05551947452300254, 7.504864834147113584 ) ) ;
#3598=CARTESIAN_POINT ( 'NONE',  ( -12.15653940608521566, -15.58205587995076868, -1.500000000000002220 ) ) ;
#3600=CARTESIAN_POINT ( 'NONE',  ( 9.769481717609929561, -17.74358427669893956, 11.49999999999999645 ) ) ;
#3604=EDGE_LOOP ( 'NONE', ( #45589, #42466, #63252, #15716 ) ) ;
#3605=CARTESIAN_POINT ( 'NONE',  ( -67.52287095715009002, -24.51387760970725083, 9.387446482453412955 ) ) ;
#3610=CARTESIAN_POINT ( 'NONE',  ( -71.62287095715005592, -24.64898659630528854, 1.056161002820824368 ) ) ;
#3611=CARTESIAN_POINT ( 'NONE',  ( -12.65591448191638335, 15.52279176289047236, -1.500000000000002220 ) ) ;
#3614=EDGE_CURVE ( 'NONE', #63089, #50699, #90430, .T. ) ;
#3615=CARTESIAN_POINT ( 'NONE',  ( -50.38822539166533687, -25.31297217564049973, 4.736250530714762874 ) ) ;
#3616=B_SPLINE_CURVE_WITH_KNOTS ( 'NONE', 3,
 ( #40302, #72261, #64670, #17454 ),
 .UNSPECIFIED., .F., .F.,
 ( 4, 4 ),
 ( 0.000000000000000000, 9.999999999997510880E-05 ),
 .UNSPECIFIED. ) ;
#3617=VECTOR ( 'NONE', #75065, 1000.000000000000114 ) ;
#3618=CARTESIAN_POINT ( 'NONE',  ( -35.62660857665062508, -24.92564183028978775, 1.928384488918258199 ) ) ;
#3619=LINE ( 'NONE', #34566, #98862 ) ;
#3622=CARTESIAN_POINT ( 'NONE',  ( -73.60709162415560058, -23.48783264082477018, -1.443836473390094355 ) ) ;
#3625=ORIENTED_EDGE ( 'NONE', *, *, #37313, .T. ) ;
#3626=CARTESIAN_POINT ( 'NONE',  ( -18.23349369547262810, -8.965252873808195133, 11.49999999999998934 ) ) ;
#3628=EDGE_CURVE ( 'NONE', #14971, #11757, #58999, .T. ) ;
#3629=CARTESIAN_POINT ( 'NONE',  ( -3.987988226355533072, 22.59150145119509290, -1.500000000000002220 ) ) ;
#3631=VERTEX_POINT ( 'NONE', #72144 ) ;
#3633=CARTESIAN_POINT ( 'NONE',  ( -49.27841808360716414, -25.26263977505040970, 6.176812849117304438 ) ) ;
#3634=AXIS2_PLACEMENT_3D ( 'NONE', #25393, #86788, #33015 ) ;
#3635=DIRECTION ( 'NONE',  ( -3.773278334453080206E-23, 0.9999999999976377785, 2.173523156925979975E-06 ) ) ;
#3636=CARTESIAN_POINT ( 'NONE',  ( 4.708956132399880978, 20.65895737721473679, 11.49999999999999645 ) ) ;
#3638=CARTESIAN_POINT ( 'NONE',  ( -18.12599551585701008, -12.76988789260850332, 11.49999999999998934 ) ) ;
#3639=ADVANCED_FACE ( 'NONE', ( #93797 ), #68419, .T. ) ;
#3640=CARTESIAN_POINT ( 'NONE',  ( 9.149160795417088821, -18.46424698110740437, 11.49999999999998934 ) ) ;
#3642=DIRECTION ( 'NONE',  ( -1.000000000000000000, -3.773278334444167608E-23, -8.201307833595939069E-29 ) ) ;
#3644=CARTESIAN_POINT ( 'NONE',  ( -54.49654312574512005, -24.34968618360932879, 0.1864209137778771175 ) ) ;
#3646=EDGE_LOOP ( 'NONE', ( #82728, #89777, #82234, #88904 ) ) ;
#3647=EDGE_LOOP ( 'NONE', ( #46761, #68544, #30198, #30 ) ) ;
#3648=VERTEX_POINT ( 'NONE', #9064 ) ;
#3650=CARTESIAN_POINT ( 'NONE',  ( -70.62287095715005592, -25.00182538069145011, 7.747789668545097541 ) ) ;
#3651=CARTESIAN_POINT ( 'NONE',  ( -108.5562042904833788, -24.65952944569304961, 1.056160979905704345 ) ) ;
#3653=CARTESIAN_POINT ( 'NONE',  ( -16.26442346200556344, 12.93145763113255775, -1.500000000000002220 ) ) ;
#3655=CARTESIAN_POINT ( 'NONE',  ( 10.00111611332133421, -19.26892646806700071, 11.49999999999999645 ) ) ;
#3656=EDGE_LOOP ( 'NONE', ( #33104, #54476, #26850, #75271 ) ) ;
#3658=CARTESIAN_POINT ( 'NONE',  ( -115.5500786810796257, -25.00158670708910691, 2.256160236439219258 ) ) ;
#3659=CARTESIAN_POINT ( 'NONE',  ( 17.95543856985664277, -13.40637504462900331, 11.49999999999998934 ) ) ;
#3660=CARTESIAN_POINT ( 'NONE',  ( -59.62287095715004881, -24.64898659630367916, 1.056161002820822592 ) ) ;
#3665=B_SPLINE_SURFACE_WITH_KNOTS ( 'NONE', 3, 3, ( 
 ( #25315, #3493, #24316, #64914 ),
 ( #87214, #9093, #64413, #48679 ),
 ( #78584, #17203, #1993, #10093 ),
 ( #41052, #41556, #49671, #95331 ),
 ( #56791, #2997, #87725, #18207 ),
 ( #80104, #16701, #10589, #47669 ),
 ( #40046, #72504, #32433, #33935 ) ),
 .UNSPECIFIED., .F., .F., .F.,
 ( 4, 3, 4 ),
 ( 4, 4 ),
 ( 0.7945040050992244751, 0.8970133687736503436, 0.9995227324480763231 ),
 ( 0.6396565428357663396, 0.6409645752979864497 ),
 .UNSPECIFIED. ) ;
#3666=ORIENTED_EDGE ( 'NONE', *, *, #10467, .F. ) ;
#3667=ORIENTED_EDGE ( 'NONE', *, *, #37561, .F. ) ;
#3669=VERTEX_POINT ( 'NONE', #39010 ) ;
#3671=CARTESIAN_POINT ( 'NONE',  ( -16.84575021678815432, -12.90291372800108505, -1.500000000000002220 ) ) ;
#3672=ORIENTED_EDGE ( 'NONE', *, *, #94562, .T. ) ;
#3673=CARTESIAN_POINT ( 'NONE',  ( -88.58843689727572723, -24.34968618360934656, 0.1864209137778829184 ) ) ;
#3674=CARTESIAN_POINT ( 'NONE',  ( 0.003323472525107682655, -21.86402403546210493, -1.500000000000002220 ) ) ;
#3675=CARTESIAN_POINT ( 'NONE',  ( -52.63895323655680869, -24.15620529776627734, 10.23563542870661003 ) ) ;
#3676=CARTESIAN_POINT ( 'NONE',  ( -22.58250372949163420, -2.080990182559540269, 11.49999999999998934 ) ) ;
#3677=CARTESIAN_POINT ( 'NONE',  ( -40.49257998994310270, -25.18430871546432925, 3.294941901647467031 ) ) ;
#3678=FACE_OUTER_BOUND ( 'NONE', #58984, .T. ) ;
#3679=CARTESIAN_POINT ( 'NONE',  ( -13.92312151449838531, -16.86485062357919773, -1.500000000000002220 ) ) ;
#3680=CARTESIAN_POINT ( 'NONE',  ( -109.5228709571500474, -24.51387760970725793, 9.387446482453411178 ) ) ;
#3681=VERTEX_POINT ( 'NONE', #78056 ) ;
#3682=DIRECTION ( 'NONE',  ( 0.000000000000000000, 2.173523156925979975E-06, -0.9999999999976378895 ) ) ;
#3683=CARTESIAN_POINT ( 'NONE',  ( -49.21454750704995007, -25.12782705690641549, 7.069183625445169206 ) ) ;
#3685=CARTESIAN_POINT ( 'NONE',  ( -90.62287095715005592, -24.92579138211019796, 1.929029949965665125 ) ) ;
#3686=B_SPLINE_CURVE_WITH_KNOTS ( 'NONE', 3,
 ( #8564, #100381, #54250, #39513, #70464, #53748 ),
 .UNSPECIFIED., .F., .F.,
 ( 4, 2, 4 ),
 ( 0.000000000000000000, 0.001380901958385392448, 0.002761803916770784895 ),
 .UNSPECIFIED. ) ;
#3687=ORIENTED_EDGE ( 'NONE', *, *, #88725, .F. ) ;
#3689=CARTESIAN_POINT ( 'NONE',  ( -89.62287095715004170, -23.48786465467241413, 11.44779295918254114 ) ) ;
#3690=CARTESIAN_POINT ( 'NONE',  ( -30.60890090734109137, -24.57171501248768664, 0.8294870405985493855 ) ) ;
#3691=CARTESIAN_POINT ( 'NONE',  ( 19.37530031839547107, -8.734557088507903799, 11.49999999999998934 ) ) ;
#3692=CARTESIAN_POINT ( 'NONE',  ( -125.6228709571500843, -25.00182538069146432, 7.747789668545100206 ) ) ;
#3693=CARTESIAN_POINT ( 'NONE',  ( -26.25750150876569933, -24.97064684238840115, 3.573366137800960907 ) ) ;
#3694=CARTESIAN_POINT ( 'NONE',  ( -85.62495650507575817, -24.92564183028979130, 1.928384488918251982 ) ) ;
#3695=CARTESIAN_POINT ( 'NONE',  ( -108.9228709571500389, -23.47596703998600631, 11.44779298504227860 ) ) ;
#3696=CARTESIAN_POINT ( 'NONE',  ( 13.61561175257155298, 13.87280521877887018, 11.49999999999998934 ) ) ;
#3699=ORIENTED_EDGE ( 'NONE', *, *, #63090, .T. ) ;
#3700=CARTESIAN_POINT ( 'NONE',  ( 3.528372621398383924, 19.26332229581237598, 11.49999999999999645 ) ) ;
#3702=CARTESIAN_POINT ( 'NONE',  ( -47.52287095715006160, -24.64965694238406613, 8.947790433994203596 ) ) ;
#3706=CARTESIAN_POINT ( 'NONE',  ( -106.5228709571500900, -23.47593901973090524, -1.443836447538996204 ) ) ;
#3707=B_SPLINE_CURVE_WITH_KNOTS ( 'NONE', 3,
 ( #4821, #82925, #35774, #66744 ),
 .UNSPECIFIED., .F., .F.,
 ( 4, 4 ),
 ( 0.000000000000000000, 9.999999999997510880E-05 ),
 .UNSPECIFIED. ) ;
#3708=VECTOR ( 'NONE', #35151, 1000.000000000000114 ) ;
#3709=CARTESIAN_POINT ( 'NONE',  ( -60.52287095715008292, -23.48783264082477018, -1.443836473390092801 ) ) ;
#3710=CARTESIAN_POINT ( 'NONE',  ( 19.18734209777730015, 4.435579877058994036, 11.49999999999998934 ) ) ;
#3712=ORIENTED_EDGE ( 'NONE', *, *, #2318, .F. ) ;
#3713=CARTESIAN_POINT ( 'NONE',  ( -94.62287095715005592, -24.50216790748205753, 0.6166512839542525048 ) ) ;
#3714=DIRECTION ( 'NONE',  ( -1.000000000000000000, -3.773278334444167608E-23, -8.201307833595939069E-29 ) ) ;
#3715=EDGE_CURVE ( 'NONE', #76130, #19368, #3300, .T. ) ;
#3718=B_SPLINE_CURVE_WITH_KNOTS ( 'NONE', 3,
 ( #93799, #38514, #40531, #62363 ),
 .UNSPECIFIED., .F., .F.,
 ( 4, 4 ),
 ( 1.387778780781445521E-17, 9.999999999997510880E-05 ),
 .UNSPECIFIED. ) ;
#3721=FACE_OUTER_BOUND ( 'NONE', #14689, .T. ) ;
#3723=CARTESIAN_POINT ( 'NONE',  ( -97.56098245220201193, -23.48786465467241413, 11.44779295918254469 ) ) ;
#3725=EDGE_CURVE ( 'NONE', #40253, #23306, #8130, .T. ) ;
#3726=CARTESIAN_POINT ( 'NONE',  ( -73.52287095715007581, -24.66019654487199730, 8.947790411086121054 ) ) ;
#3727=CARTESIAN_POINT ( 'NONE',  ( -79.52287095715007581, -24.51283580621364067, 0.6167428607019781461 ) ) ;
#3728=CARTESIAN_POINT ( 'NONE',  ( 16.79105032741591330, -10.77411451815220822, 11.49999999999998934 ) ) ;
#3729=CARTESIAN_POINT ( 'NONE',  ( -0.04038319741709193306, -22.52720777467708757, 8.529593833415562543 ) ) ;
#3730=CARTESIAN_POINT ( 'NONE',  ( -17.31707178780640533, -9.736581320607820444, -1.500000000000002220 ) ) ;
#3731=VERTEX_POINT ( 'NONE', #58249 ) ;
#3732=EDGE_CURVE ( 'NONE', #34120, #55445, #26282, .T. ) ;
#3734=ADVANCED_FACE ( 'NONE', ( #34906 ), #42033, .F. ) ;
#3735=ADVANCED_FACE ( 'NONE', ( #66372 ), #34406, .F. ) ;
#3736=LINE ( 'NONE', #60406, #41410 ) ;
#3738=CARTESIAN_POINT ( 'NONE',  ( 17.70469293622815243, 10.90570606759641592, 11.49999999999999645 ) ) ;
#3741=CARTESIAN_POINT ( 'NONE',  ( 12.51456667378993259, 19.11410217522374921, 11.49999999999999645 ) ) ;
#3743=B_SPLINE_SURFACE_WITH_KNOTS ( 'NONE', 3, 3, ( 
 ( #22905, #15313, #77203, #103 ),
 ( #31041, #92937, #62008, #54397 ),
 ( #85839, #32050, #8219, #78212 ),
 ( #8722, #39658, #70616, #33061 ),
 ( #72133, #24933, #94953, #48798 ),
 ( #10724, #88347, #26943, #64038 ),
 ( #86833, #41686, #96452, #3124 ),
 ( #49299, #95952, #1615, #71123 ),
 ( #3618, #55911, #25941, #94451 ),
 ( #34062, #40170, #56913, #32551 ) ),
 .UNSPECIFIED., .F., .F., .F.,
 ( 4, 3, 3, 4 ),
 ( 4, 4 ),
 ( 0.0004766839783833132119, 0.1491231665100180015, 0.2234464077758353540, 0.2977696490416527064 ),
 ( 0.9496086901223659282, 0.9511872814519944930 ),
 .UNSPECIFIED. ) ;
#3744=CARTESIAN_POINT ( 'NONE',  ( -55.52287095715008292, -23.47593901973090169, -1.443836447538997092 ) ) ;
#3745=CARTESIAN_POINT ( 'NONE',  ( -91.22287095715005023, -23.47596703998600276, 11.44779298504227860 ) ) ;
#3747=CARTESIAN_POINT ( 'NONE',  ( 20.24638344296597836, 0.1212440198127159030, -1.500000000000002220 ) ) ;
#3748=EDGE_CURVE ( 'NONE', #35109, #12184, #72979, .T. ) ;
#3750=CARTESIAN_POINT ( 'NONE',  ( -39.62287095715005592, -29.50250243563736774, 8.947779886222148704 ) ) ;
#3752=CARTESIAN_POINT ( 'NONE',  ( -82.55620429048340725, -24.66019654487199730, 8.947790411086128159 ) ) ;
#3753=EDGE_LOOP ( 'NONE', ( #47082, #50777, #71707, #72182 ) ) ;
#3754=DIRECTION ( 'NONE',  ( -3.773278334453080206E-23, 0.9999999999976377785, 2.173523156925979975E-06 ) ) ;
#3756=CARTESIAN_POINT ( 'NONE',  ( -1.415466703587968667, 19.98303252902060834, -1.500000000000002220 ) ) ;
#3758=CARTESIAN_POINT ( 'NONE',  ( 12.99892964944760543, 16.54660993828877125, 11.49999999999999645 ) ) ;
#3759=CARTESIAN_POINT ( 'NONE',  ( -29.76904096422576274, -25.22379592436849194, 5.866293395515224773 ) ) ;
#3761=CARTESIAN_POINT ( 'NONE',  ( 3.837975233861466329, 21.70421690940786874, -1.500000000000002220 ) ) ;
#3762=EDGE_CURVE ( 'NONE', #55465, #25617, #25003, .T. ) ;
#3763=CARTESIAN_POINT ( 'NONE',  ( -53.52287095715006870, -24.64965694238574656, 8.947790433994203596 ) ) ;
#3764=DIRECTION ( 'NONE',  ( -3.773278334453079030E-23, 0.9999999999976377785, 2.173523156925979128E-06 ) ) ;
#3765=CARTESIAN_POINT ( 'NONE',  ( -127.5228709571500616, -24.64965694238408034, 8.947790433994189385 ) ) ;
#3767=CARTESIAN_POINT ( 'NONE',  ( -91.15361000704896810, -25.27880950044357178, 5.947789066507965572 ) ) ;
#3768=CARTESIAN_POINT ( 'NONE',  ( -31.47684055086448396, -24.65952944569304250, 1.056160979905695463 ) ) ;
#3770=ORIENTED_EDGE ( 'NONE', *, *, #26761, .F. ) ;
#3771=CARTESIAN_POINT ( 'NONE',  ( -80.52287095715007581, -23.48783264082477018, -1.443836473390091246 ) ) ;
#3772=CARTESIAN_POINT ( 'NONE',  ( -61.35927149850876816, -25.04662945190125001, 7.499198004902734915 ) ) ;
#3773=CARTESIAN_POINT ( 'NONE',  ( -90.25931482958500851, -25.31788868711539209, 4.644810524077565006 ) ) ;
#3774=CARTESIAN_POINT ( 'NONE',  ( 12.93548710985481698, 15.95582723538240266, -1.500000000000002220 ) ) ;
#3775=EDGE_CURVE ( 'NONE', #99074, #82884, #43181, .T. ) ;
#3779=CARTESIAN_POINT ( 'NONE',  ( -83.52287095715007581, -23.48783264082477018, -1.443836473390090802 ) ) ;
#3780=CARTESIAN_POINT ( 'NONE',  ( 21.63714550250683644, -5.416328558471028565, 11.49999999999998934 ) ) ;
#3784=PLANE ( 'NONE',  #10824 ) ;
#3786=ADVANCED_FACE ( 'NONE', ( #35897 ), #51362, .T. ) ;
#3787=CARTESIAN_POINT ( 'NONE',  ( -32.62287095715006302, -23.47596703998600276, 11.44779298504227505 ) ) ;
#3788=DIRECTION ( 'NONE',  ( -3.773278334453080206E-23, 0.9999999999976377785, 2.173523156925979975E-06 ) ) ;
#3789=CARTESIAN_POINT ( 'NONE',  ( -20.80165436122882383, -1.723964017131293103, 11.49999999999998934 ) ) ;
#3790=ORIENTED_EDGE ( 'NONE', *, *, #66935, .F. ) ;
#3791=CARTESIAN_POINT ( 'NONE',  ( -92.58953762381672448, -24.65952944569304606, 1.056160979905705455 ) ) ;
#3792=ORIENTED_EDGE ( 'NONE', *, *, #28294, .F. ) ;
#3793=ORIENTED_EDGE ( 'NONE', *, *, #8987, .F. ) ;
#3794=VECTOR ( 'NONE', #30757, 1000.000000000000114 ) ;
#3795=CARTESIAN_POINT ( 'NONE',  ( -70.34543693012690824, -25.25935350734801332, 7.563173724185935143 ) ) ;
#3796=CARTESIAN_POINT ( 'NONE',  ( -10.38599875782317206, -18.32754119035049101, -1.500000000000002220 ) ) ;
#3800=CARTESIAN_POINT ( 'NONE',  ( -79.52287095715006160, -29.50247984919015209, -1.443849546365053582 ) ) ;
#3802=CARTESIAN_POINT ( 'NONE',  ( -76.63010253711489383, -24.35071581493543036, 9.817618358456028815 ) ) ;
#3804=CARTESIAN_POINT ( 'NONE',  ( 21.38347125639554136, -3.707035686939989638, -1.500000000000002220 ) ) ;
#3806=CARTESIAN_POINT ( 'NONE',  ( -19.83904684311861644, 10.14288308415042827, 11.49999999999999645 ) ) ;
#3808=B_SPLINE_CURVE_WITH_KNOTS ( 'NONE', 3,
 ( #24763, #99876, #69947, #55747, #48127, #79055, #80062, #88183, #57742, #96291, #64370, #41010, #3456, #2447, #79562, #32895 ),
 .UNSPECIFIED., .F., .F.,
 ( 4, 2, 2, 2, 2, 2, 2, 4 ),
 ( 8.673617379884035472E-19, 0.0002758817178494569707, 0.0005517634356989130741, 0.0008276451535483693401, 0.001103526871397825281, 0.001655290307096738463, 0.001931172024946204921, 0.002207053742795670945 ),
 .UNSPECIFIED. ) ;
#3809=CARTESIAN_POINT ( 'NONE',  ( -50.92793838057655620, -25.24728748494000286, 5.312585385865816079 ) ) ;
#3811=PLANE ( 'NONE',  #39139 ) ;
#3812=ORIENTED_EDGE ( 'NONE', *, *, #79298, .F. ) ;
#3813=B_SPLINE_CURVE_WITH_KNOTS ( 'NONE', 3,
 ( #22038, #99167, #22531, #29666 ),
 .UNSPECIFIED., .F., .F.,
 ( 4, 4 ),
 ( 0.000000000000000000, 9.999999999998897304E-05 ),
 .UNSPECIFIED. ) ;
#3814=CARTESIAN_POINT ( 'NONE',  ( -105.2228709571500787, -23.47596703998600631, 11.44779298504227860 ) ) ;
#3816=VERTEX_POINT ( 'NONE', #13085 ) ;
#3818=CARTESIAN_POINT ( 'NONE',  ( -49.87852880094167318, -25.29918105047413945, 4.602234888658000678 ) ) ;
#3820=CARTESIAN_POINT ( 'NONE',  ( -105.5228709571500616, -23.85196035786900026, -0.8779234886475166810 ) ) ;
#3821=ORIENTED_EDGE ( 'NONE', *, *, #53001, .T. ) ;
#3822=CARTESIAN_POINT ( 'NONE',  ( -130.5728709571500303, -24.93503760150525395, 8.366236236982352636 ) ) ;
#3823=CARTESIAN_POINT ( 'NONE',  ( -19.78178409256797465, 10.57734301857266246, -1.500000000000002220 ) ) ;
#3825=CARTESIAN_POINT ( 'NONE',  ( -72.55620429048340725, -23.48783264082478794, -1.443836473390067487 ) ) ;
#3826=VECTOR ( 'NONE', #84899, 1000.000000000000114 ) ;
#3827=LINE ( 'NONE', #34273, #88023 ) ;
#3829=CARTESIAN_POINT ( 'NONE',  ( -34.52287095715006160, -29.50247984919015209, -1.443849546365062242 ) ) ;
#3830=CARTESIAN_POINT ( 'NONE',  ( -130.5728709571501156, -24.82935162629097547, 1.633150109380539172 ) ) ;
#3831=CARTESIAN_POINT ( 'NONE',  ( 18.24213732562919787, -7.162457363581539838, -1.500000000000002220 ) ) ;
#3833=DIRECTION ( 'NONE',  ( 0.000000000000000000, -0.9999999999976377785, -2.173523156925979128E-06 ) ) ;
#3835=CARTESIAN_POINT ( 'NONE',  ( 13.04721882220160012, 17.14300067834640373, -1.500000000000002220 ) ) ;
#3836=CARTESIAN_POINT ( 'NONE',  ( -129.6228709571500417, -24.64965695001463430, 8.947790411086117501 ) ) ;
#3837=CARTESIAN_POINT ( 'NONE',  ( -70.86754458488196917, -25.25639569759052705, 6.955654243306450546 ) ) ;
#3838=CARTESIAN_POINT ( 'NONE',  ( -95.62287095715002749, -25.00182538069145721, 7.747789668545097541 ) ) ;
#3840=CARTESIAN_POINT ( 'NONE',  ( -16.88208375265294237, -15.58181570610299715, -1.500000000000002220 ) ) ;
#3841=B_SPLINE_CURVE_WITH_KNOTS ( 'NONE', 3,
 ( #47342, #37722, #53466, #22972 ),
 .UNSPECIFIED., .F., .F.,
 ( 4, 4 ),
 ( 0.9211577762202510788, 0.9301642074923666126 ),
 .UNSPECIFIED. ) ;
#3844=CARTESIAN_POINT ( 'NONE',  ( -84.62287095715008434, -23.47596703998600631, 11.44779298504227860 ) ) ;
#3845=CARTESIAN_POINT ( 'NONE',  ( -49.56822730090311779, -23.48783264082477018, -1.443836473390094133 ) ) ;
#3846=CARTESIAN_POINT ( 'NONE',  ( 15.80722972286721983, -12.41807379269815215, 11.49999999999999645 ) ) ;
#3847=CARTESIAN_POINT ( 'NONE',  ( -77.52287095715006160, -29.50248528299804818, 1.056150453629038477 ) ) ;
#3850=CARTESIAN_POINT ( 'NONE',  ( -69.62287095715005592, -29.50247984919015209, -1.443849546365055359 ) ) ;
#3851=CARTESIAN_POINT ( 'NONE',  ( -79.62287095715005592, -24.64965695001468404, 8.947790433994182280 ) ) ;
#3852=DIRECTION ( 'NONE',  ( -3.773278334453079030E-23, 0.9999999999976377785, 2.173523156925979128E-06 ) ) ;
#3853=CARTESIAN_POINT ( 'NONE',  ( -19.77004505525285083, 2.005399880840008642, -1.500000000000002220 ) ) ;
#3854=ADVANCED_FACE ( 'NONE', ( #100305 ), #84105, .F. ) ;
#3855=DIRECTION ( 'NONE',  ( 3.773278334444166432E-23, -1.000000000000000000, 0.000000000000000000 ) ) ;
#3856=CARTESIAN_POINT ( 'NONE',  ( -0.6023826358649750912, 19.72334862104828090, -1.500000000000002220 ) ) ;
#3857=EDGE_CURVE ( 'NONE', #25844, #67625, #75864, .T. ) ;
#3858=CARTESIAN_POINT ( 'NONE',  ( -42.55306471323350337, -23.96119346886880663, -0.6495511937831992544 ) ) ;
#3859=EDGE_CURVE ( 'NONE', #15452, #38350, #34725, .T. ) ;
#3861=EDGE_CURVE ( 'NONE', #41110, #8126, #89185, .T. ) ;
#3864=CARTESIAN_POINT ( 'NONE',  ( -20.24099117049231467, 3.958469829285517161, 11.49999999999999645 ) ) ;
#3865=B_SPLINE_CURVE_WITH_KNOTS ( 'NONE', 3,
 ( #78902, #41362, #18018, #32235 ),
 .UNSPECIFIED., .F., .F.,
 ( 4, 4 ),
 ( 0.000000000000000000, 9.999999999999592548E-05 ),
 .UNSPECIFIED. ) ;
#3868=CARTESIAN_POINT ( 'NONE',  ( 21.71957326813621592, -6.446789169762093152, 11.49999999999999645 ) ) ;
#3870=CARTESIAN_POINT ( 'NONE',  ( -102.6228709571500559, -24.65952944569304606, 1.056160979905702124 ) ) ;
#3871=CARTESIAN_POINT ( 'NONE',  ( -50.65411740745392422, -25.31193108374115752, 4.703768078485199844 ) ) ;
#3872=VECTOR ( 'NONE', #51009, 1000.000000000000114 ) ;
#3874=CARTESIAN_POINT ( 'NONE',  ( -27.65532027823855543, -24.93063634776342141, 8.251096489757108188 ) ) ;
#3878=EDGE_CURVE ( 'NONE', #94577, #33073, #10455, .T. ) ;
#3880=CARTESIAN_POINT ( 'NONE',  ( 21.14566350062385780, -8.679158401671109857, 11.49999999999998934 ) ) ;
#3881=PLANE ( 'NONE',  #61665 ) ;
#3882=CARTESIAN_POINT ( 'NONE',  ( -113.5222245837002646, -23.48786465467241058, 11.44779295918254292 ) ) ;
#3883=PLANE ( 'NONE',  #72805 ) ;
#3884=CARTESIAN_POINT ( 'NONE',  ( -22.50818191331092777, 0.9639279967183422837, 11.49999999999999645 ) ) ;
#3886=B_SPLINE_CURVE_WITH_KNOTS ( 'NONE', 3,
 ( #2980, #50145, #49650, #33913, #95312, #3476, #34414, #65395, #71991, #64896, #72486, #80583, #96809, #63893, #42541, #73476, #56274, #3973 ),
 .UNSPECIFIED., .F., .F.,
 ( 4, 2, 2, 2, 2, 2, 2, 2, 4 ),
 ( 0.000000000000000000, 0.0001439754707682965951, 0.0002879509415365931902, 0.0005759018830731794415, 0.0008638528246097658013, 0.001151803766146352161, 0.001727705649219524664, 0.002015656590756111349, 0.002303607532292697817 ),
 .UNSPECIFIED. ) ;
#3887=CARTESIAN_POINT ( 'NONE',  ( -33.58953762381672448, -23.48786465467240347, 11.44779295918255535 ) ) ;
#3888=CARTESIAN_POINT ( 'NONE',  ( -19.44315311050126382, -10.23602577120861667, 11.49999999999998934 ) ) ;
#3889=ADVANCED_FACE ( 'NONE', ( #52166 ), #5485, .T. ) ;
#3890=PLANE ( 'NONE',  #91641 ) ;
#3891=CARTESIAN_POINT ( 'NONE',  ( -29.14051086615235420, -24.79700015330595164, 6.215525944783297341 ) ) ;
#3893=CARTESIAN_POINT ( 'NONE',  ( -63.62287095715004881, -23.95044443724992789, 10.65354141964649948 ) ) ;
#3894=CARTESIAN_POINT ( 'NONE',  ( -111.6228709571500559, -24.64898659630368627, 1.056161002820831474 ) ) ;
#3895=ORIENTED_EDGE ( 'NONE', *, *, #1374, .F. ) ;
#3896=PLANE ( 'NONE',  #24194 ) ;
#3897=CARTESIAN_POINT ( 'NONE',  ( -10.27258457790969892, -17.75692283049141196, -1.500000000000002220 ) ) ;
#3898=ORIENTED_EDGE ( 'NONE', *, *, #44188, .F. ) ;
#3899=VERTEX_POINT ( 'NONE', #69386 ) ;
#3902=CARTESIAN_POINT ( 'NONE',  ( -8.701767255460435280, 21.38705905713849020, -1.500000000000002220 ) ) ;
#3903=CARTESIAN_POINT ( 'NONE',  ( -104.5951208871063471, -23.73791477778912196, 11.05961554403170410 ) ) ;
#3904=CARTESIAN_POINT ( 'NONE',  ( -20.29798418530817017, 1.744846428065259136, -1.500000000000002220 ) ) ;
#3910=CARTESIAN_POINT ( 'NONE',  ( -89.49044893904931541, -25.11033443465437287, 2.832404802291436319 ) ) ;
#3911=CARTESIAN_POINT ( 'NONE',  ( -35.52287095715006870, -23.47593901973090169, -1.443836447538997092 ) ) ;
#3913=CARTESIAN_POINT ( 'NONE',  ( -28.94548163072471425, -25.21531839410873843, 3.108273061491439559 ) ) ;
#3914=CARTESIAN_POINT ( 'NONE',  ( -89.62287095715004170, -23.47593901973091235, -1.443836447539002865 ) ) ;
#3917=CARTESIAN_POINT ( 'NONE',  ( -8.119355292522030254, -19.11072509857415369, 11.49999999999998934 ) ) ;
#3918=EDGE_CURVE ( 'NONE', #86903, #13321, #53175, .T. ) ;
#3920=CARTESIAN_POINT ( 'NONE',  ( -101.6339284197689210, -23.73766607897670511, -1.055555164236452237 ) ) ;
#3921=ORIENTED_EDGE ( 'NONE', *, *, #52793, .T. ) ;
#3922=CARTESIAN_POINT ( 'NONE',  ( -86.62287095715008434, -24.34917612406837861, 0.1852690917426653427 ) ) ;
#3926=FACE_OUTER_BOUND ( 'NONE', #99232, .T. ) ;
#3929=CARTESIAN_POINT ( 'NONE',  ( -70.39323859381175907, -25.31201590701856574, 5.314173951595296153 ) ) ;
#3930=CARTESIAN_POINT ( 'NONE',  ( -7.692412698405892257, 20.70400481474656118, 11.49999999999999645 ) ) ;
#3932=CARTESIAN_POINT ( 'NONE',  ( -103.5909381567761898, -24.15543982623907482, -0.2315651400026619011 ) ) ;
#3933=CARTESIAN_POINT ( 'NONE',  ( 1.383477600506065164, -22.57338898373578218, -1.500000000000002220 ) ) ;
#3934=CARTESIAN_POINT ( 'NONE',  ( -115.5137987077945070, -24.92592662359561473, 8.075495903017996469 ) ) ;
#3935=VERTEX_POINT ( 'NONE', #8489 ) ;
#3937=CARTESIAN_POINT ( 'NONE',  ( -88.52287095715009002, -24.66019654487200441, 8.947790411086119278 ) ) ;
#3939=ORIENTED_EDGE ( 'NONE', *, *, #40369, .F. ) ;
#3940=CARTESIAN_POINT ( 'NONE',  ( -14.79452276021403634, 15.15755283273500531, -1.500000000000002220 ) ) ;
#3942=CARTESIAN_POINT ( 'NONE',  ( -41.82823102631974876, -25.29805763927562268, 4.565812412427879607 ) ) ;
#3943=CARTESIAN_POINT ( 'NONE',  ( 22.20884612314100792, -2.053178116692622623, -1.500000000000002220 ) ) ;
#3944=B_SPLINE_CURVE_WITH_KNOTS ( 'NONE', 3,
 ( #32438, #1501, #63412, #17715, #56299, #11097, #10595, #94330 ),
 .UNSPECIFIED., .F., .F.,
 ( 4, 2, 2, 4 ),
 ( -0.001224554619866345413, -0.0002241820295893642324, 0.0007761905606876169476, 0.002776935741241582777 ),
 .UNSPECIFIED. ) ;
#3947=CARTESIAN_POINT ( 'NONE',  ( -80.22287095715007865, -23.47596703998600631, 11.44779298504227860 ) ) ;
#3949=CARTESIAN_POINT ( 'NONE',  ( -36.61838302510732035, -23.48786465467240347, 11.44779295918255180 ) ) ;
#3951=CARTESIAN_POINT ( 'NONE',  ( -18.91883139384513157, -4.797682538509264738, 11.49999999999998934 ) ) ;
#3952=CARTESIAN_POINT ( 'NONE',  ( 15.63241172484657682, -14.69700884395465934, -1.500000000000002220 ) ) ;
#3956=CARTESIAN_POINT ( 'NONE',  ( 2.581029390964978187, -22.66945732913600509, -1.500000000000002220 ) ) ;
#3959=CARTESIAN_POINT ( 'NONE',  ( -102.6290229638939024, -24.15543982623908192, -0.2315651400026459694 ) ) ;
#3961=CARTESIAN_POINT ( 'NONE',  ( 16.68016870136555596, 10.92824754362290385, 11.49999999999999645 ) ) ;
#3962=CARTESIAN_POINT ( 'NONE',  ( -31.52287095715006160, -24.50216790748204332, 0.6166512839542445112 ) ) ;
#3964=EDGE_CURVE ( 'NONE', #45335, #94542, #23699, .T. ) ;
#3966=CARTESIAN_POINT ( 'NONE',  ( -48.63974925878575561, -24.15543982623907127, -0.2315651400026527418 ) ) ;
#3967=EDGE_LOOP ( 'NONE', ( #13290, #53434, #130, #76891 ) ) ;
#3969=CARTESIAN_POINT ( 'NONE',  ( -77.52287095715007581, -23.48783264082476308, -1.443836473390091912 ) ) ;
#3970=AXIS2_PLACEMENT_3D ( 'NONE', #99449, #77610, #29442 ) ;
#3972=CARTESIAN_POINT ( 'NONE',  ( 18.84366469573077296, 10.75509914293975555, -1.500000000000002220 ) ) ;
#3973=CARTESIAN_POINT ( 'NONE',  ( -50.40895856474225667, -25.04307398257883577, 7.563174194274489892 ) ) ;
#3974=CARTESIAN_POINT ( 'NONE',  ( -16.69004703121433408, -10.21020960635683394, -1.500000000000002220 ) ) ;
#3975=EDGE_CURVE ( 'NONE', #5790, #43961, #92756, .T. ) ;
#3978=CARTESIAN_POINT ( 'NONE',  ( -60.62287095715003460, -24.63345952396255001, 9.038047939301510070 ) ) ;
#3979=CARTESIAN_POINT ( 'NONE',  ( -20.02755620033356010, -4.236777897013602079, 11.49999999999999645 ) ) ;
#3981=CARTESIAN_POINT ( 'NONE',  ( -59.56094173781918499, -25.20074414198133539, 3.409327697718782080 ) ) ;
#3982=ORIENTED_EDGE ( 'NONE', *, *, #98674, .T. ) ;
#3983=DIRECTION ( 'NONE',  ( 0.000000000000000000, -2.173523156925979552E-06, 0.9999999999976378895 ) ) ;
#3984=PLANE ( 'NONE',  #8795 ) ;
#3986=CARTESIAN_POINT ( 'NONE',  ( -109.5126161358243309, -24.65952944569305316, 1.056160979905708786 ) ) ;
#3987=ORIENTED_EDGE ( 'NONE', *, *, #45923, .F. ) ;
#3988=B_SPLINE_CURVE_WITH_KNOTS ( 'NONE', 3,
 ( #2416, #41472, #18620, #32861 ),
 .UNSPECIFIED., .F., .F.,
 ( 4, 4 ),
 ( 0.000000000000000000, 9.999999999998897304E-05 ),
 .UNSPECIFIED. ) ;
#3989=CARTESIAN_POINT ( 'NONE',  ( 14.87233727408824713, -17.56007624320114857, 11.49999999999999645 ) ) ;
#3990=CARTESIAN_POINT ( 'NONE',  ( -22.19569011343799048, 5.130922947863589378, -1.500000000000002220 ) ) ;
#3991=CARTESIAN_POINT ( 'NONE',  ( -110.6235418037408920, -25.00182538069147498, 7.747789668545046027 ) ) ;
#3993=CARTESIAN_POINT ( 'NONE',  ( -98.22287095715007865, -23.47593901973090880, -1.443836447538997092 ) ) ;
#3996=CARTESIAN_POINT ( 'NONE',  ( -52.62287095715005592, -23.47593901973091235, -1.443836447539009749 ) ) ;
#3997=FACE_OUTER_BOUND ( 'NONE', #50876, .T. ) ;
#3998=CARTESIAN_POINT ( 'NONE',  ( 0.003323472525107682655, -21.86402403546210493, 11.49999999999998934 ) ) ;
#3999=DIRECTION ( 'NONE',  ( 3.773278334444167608E-23, -1.000000000000000000, 0.000000000000000000 ) ) ;
#4002=CARTESIAN_POINT ( 'NONE',  ( -58.54815136844473500, -24.15543982623907482, -0.2315651400026660645 ) ) ;
#4004=CARTESIAN_POINT ( 'NONE',  ( 5.143668500415711442, -19.74887971880038151, 11.49999999999998934 ) ) ;
#4005=ORIENTED_EDGE ( 'NONE', *, *, #85862, .F. ) ;
#4006=VERTEX_POINT ( 'NONE', #94718 ) ;
#4008=ORIENTED_EDGE ( 'NONE', *, *, #38247, .T. ) ;
#4009=CARTESIAN_POINT ( 'NONE',  ( -22.55714481399219906, -4.634528848986672500, -1.500000000000002220 ) ) ;
#4010=CARTESIAN_POINT ( 'NONE',  ( -79.62287095715005592, -29.50250243563736774, 8.947779886222141599 ) ) ;
#4011=CARTESIAN_POINT ( 'NONE',  ( 5.087728227403598424, 19.53446797131710611, -1.500000000000002220 ) ) ;
#4013=ADVANCED_FACE ( 'NONE', ( #77481 ), #62799, .F. ) ;
#4014=CARTESIAN_POINT ( 'NONE',  ( -97.62287095715005592, -23.48783264082478794, -1.443836473390061936 ) ) ;
#4016=CARTESIAN_POINT ( 'NONE',  ( -95.54220411708793392, -25.00158670708911046, 2.256160236439221034 ) ) ;
#4017=CARTESIAN_POINT ( 'NONE',  ( -117.6228709571500559, -29.50250243563736774, 8.947779886222134493 ) ) ;
#4018=CARTESIAN_POINT ( 'NONE',  ( 16.75108703964928480, -13.32659110743468212, 11.49999999999999645 ) ) ;
#4020=PLANE ( 'NONE',  #56605 ) ;
#4021=ORIENTED_EDGE ( 'NONE', *, *, #58225, .F. ) ;
#4022=CARTESIAN_POINT ( 'NONE',  ( -16.22183044023116238, -15.26045173261249310, 11.49999999999998934 ) ) ;
#4023=CARTESIAN_POINT ( 'NONE',  ( 15.58315679939408582, 13.61395703526229894, -1.500000000000002220 ) ) ;
#4024=ADVANCED_FACE ( 'NONE', ( #86108 ), #15588, .T. ) ;
#4029=EDGE_LOOP ( 'NONE', ( #99891, #378, #100236, #49073 ) ) ;
#4030=FACE_OUTER_BOUND ( 'NONE', #99357, .T. ) ;
#4031=ORIENTED_EDGE ( 'NONE', *, *, #53751, .T. ) ;
#4033=CARTESIAN_POINT ( 'NONE',  ( -15.18370147500227496, -14.46048895944246127, -1.500000000000002220 ) ) ;
#4034=CARTESIAN_POINT ( 'NONE',  ( -12.54888962926113827, 17.92887824059606672, 11.49999999999999645 ) ) ;
#4035=B_SPLINE_CURVE_WITH_KNOTS ( 'NONE', 3,
 ( #98516, #43753, #58490, #51868, #66617, #82305 ),
 .UNSPECIFIED., .F., .F.,
 ( 4, 2, 4 ),
 ( 1.570887131794176733E-05, 0.001396322306279756519, 0.002776935741241571502 ),
 .UNSPECIFIED. ) ;
#4037=CARTESIAN_POINT ( 'NONE',  ( -73.50726928729523024, -24.15620529776628089, 10.23563542870660470 ) ) ;
#4038=CARTESIAN_POINT ( 'NONE',  ( 12.90280524143238594, -18.44629484376132922, 11.49999999999998934 ) ) ;
#4039=CARTESIAN_POINT ( 'NONE',  ( 19.40473180639871131, -7.901900427366274293, 11.49999999999998934 ) ) ;
#4040=CARTESIAN_POINT ( 'NONE',  ( -38.49113028606867459, -24.34968618360933590, 0.1864209137778850278 ) ) ;
#4041=CARTESIAN_POINT ( 'NONE',  ( -94.62287095715005592, -29.50250243563736774, 8.947779886222139822 ) ) ;
#4042=PLANE ( 'NONE',  #9716 ) ;
#4043=CARTESIAN_POINT ( 'NONE',  ( -68.62287095715005592, -23.47593901973091235, -1.443836447539006196 ) ) ;
#4045=ORIENTED_EDGE ( 'NONE', *, *, #94115, .T. ) ;
#4047=CARTESIAN_POINT ( 'NONE',  ( -52.61349081655445303, -23.48783264082478439, -1.443836473390069708 ) ) ;
#4049=CARTESIAN_POINT ( 'NONE',  ( -19.15072323977689095, -9.709862252083167888, -1.500000000000002220 ) ) ;
#4051=ORIENTED_EDGE ( 'NONE', *, *, #83710, .F. ) ;
#4052=CARTESIAN_POINT ( 'NONE',  ( 20.77832821955112408, -3.674247523096572099, -1.500000000000002220 ) ) ;
#4054=DIRECTION ( 'NONE',  ( -3.773278334453079618E-23, 0.9999999999976377785, 2.173523156925979975E-06 ) ) ;
#4055=CARTESIAN_POINT ( 'NONE',  ( -50.52198862043362482, -23.48786465467240347, 11.44779295918255002 ) ) ;
#4056=CARTESIAN_POINT ( 'NONE',  ( -80.88924702628075636, -25.30877091901892939, 4.592921212922877139 ) ) ;
#4057=CARTESIAN_POINT ( 'NONE',  ( -129.5557415901027980, -24.51419770103158413, 9.386484678747176957 ) ) ;
#4058=CARTESIAN_POINT ( 'NONE',  ( 18.18892703665305177, -12.56521834855340281, -1.500000000000002220 ) ) ;
#4059=ORIENTED_EDGE ( 'NONE', *, *, #25399, .T. ) ;
#4060=CARTESIAN_POINT ( 'NONE',  ( -109.5948960647422581, -25.14264220134220196, 6.986250900936221697 ) ) ;
#4062=CARTESIAN_POINT ( 'NONE',  ( -41.71489324084514294, -25.31624590159391985, 4.846374443859488679 ) ) ;
#4063=EDGE_CURVE ( 'NONE', #63440, #86142, #15291, .T. ) ;
#4064=CARTESIAN_POINT ( 'NONE',  ( -26.94960779665208861, -25.02909261677565311, 3.798368663089755515 ) ) ;
#4065=VECTOR ( 'NONE', #35172, 1000.000000000000114 ) ;
#4066=CARTESIAN_POINT ( 'NONE',  ( -102.5228709571500900, -23.47593901973090524, -1.443836447538996648 ) ) ;
#4067=CARTESIAN_POINT ( 'NONE',  ( 20.50650179695670872, -5.950058665555418180, 11.49999999999998934 ) ) ;
#4068=CARTESIAN_POINT ( 'NONE',  ( -69.07465920187155461, -25.18135671409043397, 6.806830623293391724 ) ) ;
#4069=CARTESIAN_POINT ( 'NONE',  ( -66.62287095715005592, -24.64898659630367916, 1.056161002820824368 ) ) ;
#4070=CARTESIAN_POINT ( 'NONE',  ( -84.55620429048337883, -24.66019654487199730, 8.947790411086124607 ) ) ;
#4072=CARTESIAN_POINT ( 'NONE',  ( 17.82461400791848405, -13.82690402418615960, -1.500000000000002220 ) ) ;
#4073=CARTESIAN_POINT ( 'NONE',  ( -102.5228709571501042, -23.96127896942128999, -0.6493128930940196275 ) ) ;
#4075=DIRECTION ( 'NONE',  ( -3.773278334444166432E-23, 1.000000000000000000, 0.000000000000000000 ) ) ;
#4076=CARTESIAN_POINT ( 'NONE',  ( -79.55429618991367136, -23.96119346886880308, -0.6495511937832122440 ) ) ;
#4077=CARTESIAN_POINT ( 'NONE',  ( 12.09797951242163805, 15.59582292391970704, 11.49999999999999645 ) ) ;
#4078=CARTESIAN_POINT ( 'NONE',  ( -82.62287095715005592, -23.72773821059536559, 11.05748984161097503 ) ) ;
#4080=CARTESIAN_POINT ( 'NONE',  ( -67.54036089741288151, -24.51314013834315375, 0.6176544820404126224 ) ) ;
#4082=DIRECTION ( 'NONE',  ( 0.000000000000000000, -0.9999999999976377785, -2.173523156925979975E-06 ) ) ;
#4083=CARTESIAN_POINT ( 'NONE',  ( -29.40205842853959339, -25.26026517658197434, 2.693429348280085289 ) ) ;
#4084=EDGE_CURVE ( 'NONE', #16907, #74034, #58912, .T. ) ;
#4085=CARTESIAN_POINT ( 'NONE',  ( -75.52287095715006160, -24.15516710230293640, 10.28746687063726029 ) ) ;
#4086=CARTESIAN_POINT ( 'NONE',  ( -9.004746288917990782, -19.65190454534591069, -1.500000000000002220 ) ) ;
#4087=CARTESIAN_POINT ( 'NONE',  ( -126.6228709571500843, -23.47596703998600631, 11.44779298504227860 ) ) ;
#4090=CARTESIAN_POINT ( 'NONE',  ( -92.62287095715005592, -23.48783264082479150, -1.443836473390063713 ) ) ;
#4091=CARTESIAN_POINT ( 'NONE',  ( -90.62287095715004170, -29.50248789122583659, 2.256150453626215580 ) ) ;
#4092=CARTESIAN_POINT ( 'NONE',  ( -6.431973572030615038, 18.70533856667250916, 11.49999999999998934 ) ) ;
#4094=EDGE_CURVE ( 'NONE', #55468, #17140, #46873, .T. ) ;
#4095=CARTESIAN_POINT ( 'NONE',  ( -12.33117494125061242, 16.09929768045241261, 11.49999999999999645 ) ) ;
#4096=LINE ( 'NONE', #59377, #58608 ) ;
#4097=EDGE_CURVE ( 'NONE', #73872, #803, #66293, .T. ) ;
#4099=CARTESIAN_POINT ( 'NONE',  ( -43.62287095715004170, -23.48786465467241058, 11.44779295918255180 ) ) ;
#4103=DIRECTION ( 'NONE',  ( 1.000000000000000000, 3.773278334444166432E-23, 8.201307841325785021E-29 ) ) ;
#4104=CARTESIAN_POINT ( 'NONE',  ( -52.58953762381672448, -24.64898659630367561, 1.056161002820380723 ) ) ;
#4106=CARTESIAN_POINT ( 'NONE',  ( -8.782848147209532996, 18.00178819457707746, 11.49999999999998934 ) ) ;
#4112=CARTESIAN_POINT ( 'NONE',  ( -51.52287095715006870, -24.51283580621365132, 0.6167428607019705966 ) ) ;
#4113=CARTESIAN_POINT ( 'NONE',  ( -115.5895376238166961, -23.48783264082478794, -1.443836473390058384 ) ) ;
#4115=CARTESIAN_POINT ( 'NONE',  ( -105.5228709571500616, -24.62226745350437440, 0.9660975649728157366 ) ) ;
#4116=CARTESIAN_POINT ( 'NONE',  ( -73.54547332343318544, -24.34968618360933590, 0.1864209137778806424 ) ) ;
#4118=CARTESIAN_POINT ( 'NONE',  ( -51.53971197011429695, -25.29440776045720085, 5.833784451200526355 ) ) ;
#4120=CARTESIAN_POINT ( 'NONE',  ( 12.41260344771940360, 16.11316662856288318, 11.49999999999998934 ) ) ;
#4123=CARTESIAN_POINT ( 'NONE',  ( -22.60589916338503613, 3.847557683979087706, 11.49999999999998934 ) ) ;
#4126=CARTESIAN_POINT ( 'NONE',  ( -89.58953762381671027, -23.48783264082478439, -1.443836473390063713 ) ) ;
#4127=CARTESIAN_POINT ( 'NONE',  ( -49.58282627629191808, -25.26264116536357562, 6.816471629502625973 ) ) ;
#4128=ADVANCED_FACE ( 'NONE', ( #18100 ), #72899, .T. ) ;
#4130=CARTESIAN_POINT ( 'NONE',  ( -21.01389645921736360, -2.595061309317715281, 11.49999999999999645 ) ) ;
#4132=CARTESIAN_POINT ( 'NONE',  ( -19.06252244145942498, 11.34236556261432405, 11.49999999999998934 ) ) ;
#4133=EDGE_CURVE ( 'NONE', #81499, #82077, #4878, .T. ) ;
#4134=CARTESIAN_POINT ( 'NONE',  ( 18.07347782881280907, 9.871946371954690491, -1.500000000000002220 ) ) ;
#4135=ORIENTED_EDGE ( 'NONE', *, *, #31925, .F. ) ;
#4136=LINE ( 'NONE', #26964, #45818 ) ;
#4138=PLANE ( 'NONE',  #67344 ) ;
#4140=CARTESIAN_POINT ( 'NONE',  ( -50.52287095715006160, -23.47596703998600631, 11.44779298504229104 ) ) ;
#4142=EDGE_LOOP ( 'NONE', ( #60180, #79891, #545, #99105 ) ) ;
#4145=CARTESIAN_POINT ( 'NONE',  ( -28.56161880046136758, -23.57756926196503855, 11.05961558438220926 ) ) ;
#4147=CARTESIAN_POINT ( 'NONE',  ( -8.119355292522030254, -19.11072509857415369, -1.500000000000002220 ) ) ;
#4148=CARTESIAN_POINT ( 'NONE',  ( 20.57166443188586769, -7.073620337204646447, 11.49999999999999645 ) ) ;
#4149=EDGE_CURVE ( 'NONE', #89671, #89470, #81503, .T. ) ;
#4150=ORIENTED_EDGE ( 'NONE', *, *, #71672, .F. ) ;
#4152=CARTESIAN_POINT ( 'NONE',  ( -115.5143242223860653, -24.83618233451450408, 1.606449574219536824 ) ) ;
#4153=CARTESIAN_POINT ( 'NONE',  ( -14.39434090420295220, 17.20869321163716492, 11.49999999999998934 ) ) ;
#4154=CARTESIAN_POINT ( 'NONE',  ( -33.58953762381673158, -24.64965694238406613, 8.947790433994663672 ) ) ;
#4156=ORIENTED_EDGE ( 'NONE', *, *, #81969, .F. ) ;
#4157=CARTESIAN_POINT ( 'NONE',  ( -61.52287095715007581, -23.48783264082476308, -1.443836473390092356 ) ) ;
#4159=EDGE_LOOP ( 'NONE', ( #44449, #40971, #10628, #75618 ) ) ;
#4161=CARTESIAN_POINT ( 'NONE',  ( -69.62287095715005592, -24.35013146730203459, 9.818937971375111928 ) ) ;
#4165=CARTESIAN_POINT ( 'NONE',  ( -21.25539211000977957, 0.9166567589900279645, -1.500000000000002220 ) ) ;
#4166=VERTEX_POINT ( 'NONE', #97716 ) ;
#4167=CARTESIAN_POINT ( 'NONE',  ( -88.56233851268359558, -23.48783264082476663, -1.443836473390093467 ) ) ;
#4168=CARTESIAN_POINT ( 'NONE',  ( -6.661741538832703036, 20.79550341630197607, 11.49999999999998934 ) ) ;
#4169=CARTESIAN_POINT ( 'NONE',  ( -38.52287095715006870, -24.64965694238406613, 8.947790433994205372 ) ) ;
#4170=CARTESIAN_POINT ( 'NONE',  ( -19.30582015231555104, -11.89196067722419237, -1.500000000000002220 ) ) ;
#4171=CARTESIAN_POINT ( 'NONE',  ( -112.5562042904834072, -24.65952944569304961, 1.056160979905706565 ) ) ;
#4173=DIRECTION ( 'NONE',  ( -3.773278334453079618E-23, 0.9999999999976377785, 2.173523156925978705E-06 ) ) ;
#4174=CARTESIAN_POINT ( 'NONE',  ( -3.281320334969873631, 21.64054093270537393, -1.500000000000002220 ) ) ;
#4181=ORIENTED_EDGE ( 'NONE', *, *, #95955, .T. ) ;
#4183=ORIENTED_EDGE ( 'NONE', *, *, #42918, .F. ) ;
#4185=CARTESIAN_POINT ( 'NONE',  ( -30.63911803361059683, -23.78088414657023719, -0.9709657327914291702 ) ) ;
#4186=CARTESIAN_POINT ( 'NONE',  ( -0.06837171988653999166, -21.26218376953697486, -1.500000000000002220 ) ) ;
#4188=CARTESIAN_POINT ( 'NONE',  ( -27.08002768120591242, -24.97064435294952389, 2.428018831443120806 ) ) ;
#4189=CARTESIAN_POINT ( 'NONE',  ( -85.58227612371159410, -24.92564183028979130, 1.928384488918251982 ) ) ;
#4190=DIRECTION ( 'NONE',  ( -1.000000000000000000, -3.773278334444167020E-23, -8.201307811038811694E-29 ) ) ;
#4191=CARTESIAN_POINT ( 'NONE',  ( -79.62287095715004170, -23.72773821059535848, 11.05748984161097681 ) ) ;
#4192=ORIENTED_EDGE ( 'NONE', *, *, #19918, .F. ) ;
#4193=CARTESIAN_POINT ( 'NONE',  ( 18.95637782189878706, 4.751392969308117387, 11.49999999999999645 ) ) ;
#4194=CARTESIAN_POINT ( 'NONE',  ( -99.36664296761678372, -25.31172790992623689, 4.689206871853577319 ) ) ;
#4195=EDGE_CURVE ( 'NONE', #11900, #54673, #40757, .T. ) ;
#4196=CARTESIAN_POINT ( 'NONE',  ( -27.79920052361254079, -24.64785536601324978, 8.250242701940406320 ) ) ;
#4197=ORIENTED_EDGE ( 'NONE', *, *, #32957, .T. ) ;
#4198=CARTESIAN_POINT ( 'NONE',  ( -71.62287095715005592, -29.50250786944525672, 11.44777988621623699 ) ) ;
#4199=CARTESIAN_POINT ( 'NONE',  ( -99.53504363246379683, -25.31439613239528441, 5.566583519096571564 ) ) ;
#4200=CARTESIAN_POINT ( 'NONE',  ( -51.62287095715005592, -23.48783264082478084, -1.443836473390070596 ) ) ;
#4201=CARTESIAN_POINT ( 'NONE',  ( -80.55728237399675606, -25.03156060684649731, 7.562285999033727890 ) ) ;
#4202=CARTESIAN_POINT ( 'NONE',  ( -5.193715590271882121, 18.98282465337476665, -1.500000000000002220 ) ) ;
#4204=EDGE_CURVE ( 'NONE', #1307, #36594, #62505, .T. ) ;
#4207=ADVANCED_FACE ( 'NONE', ( #42456 ), #27715, .F. ) ;
#4209=EDGE_LOOP ( 'NONE', ( #89853, #44560, #96420, #94817 ) ) ;
#4211=DIRECTION ( 'NONE',  ( 1.000000000000000000, 3.773278334444167608E-23, 8.201307833595939069E-29 ) ) ;
#4212=CARTESIAN_POINT ( 'NONE',  ( -55.60865610405180348, -23.85016227208578954, -0.8807180028928371929 ) ) ;
#4213=CARTESIAN_POINT ( 'NONE',  ( -118.6277876297057929, -23.73766607897671221, -1.055555164236448684 ) ) ;
#4214=CARTESIAN_POINT ( 'NONE',  ( -79.91782308976125648, -25.27183487616304447, 3.712349674769177543 ) ) ;
#4215=B_SPLINE_CURVE_WITH_KNOTS ( 'NONE', 3,
 ( #33255, #2826, #33765, #64748, #78422, #95665 ),
 .UNSPECIFIED., .F., .F.,
 ( 4, 2, 4 ),
 ( 0.000000000000000000, 0.001380901958385388545, 0.002761803916770777089 ),
 .UNSPECIFIED. ) ;
#4217=CARTESIAN_POINT ( 'NONE',  ( -79.52287095715003318, -23.73907113216989728, -1.053371485793251905 ) ) ;
#4218=CARTESIAN_POINT ( 'NONE',  ( 14.81759351585047391, 13.34335055255382052, -1.500000000000002220 ) ) ;
#4219=ADVANCED_FACE ( 'NONE', ( #4385 ), #14943, .T. ) ;
#4220=CARTESIAN_POINT ( 'NONE',  ( -0.04029912359210763989, -22.52829617641010174, 1.476849900881732625 ) ) ;
#4221=CARTESIAN_POINT ( 'NONE',  ( 3.219775368129482285, -19.64489633315863770, -1.500000000000002220 ) ) ;
#4222=EDGE_LOOP ( 'NONE', ( #71909, #90635, #30018, #33362 ) ) ;
#4224=AXIS2_PLACEMENT_3D ( 'NONE', #90568, #21539, #27184 ) ;
#4225=DIRECTION ( 'NONE',  ( 0.000000000000000000, 0.000000000000000000, 1.000000000000000000 ) ) ;
#4228=CARTESIAN_POINT ( 'NONE',  ( -37.52287095715006870, -23.47593901973090524, -1.443836447538997314 ) ) ;
#4230=CARTESIAN_POINT ( 'NONE',  ( -51.29572949068491994, -25.25925092192675336, 3.940762572495089877 ) ) ;
#4232=ORIENTED_EDGE ( 'NONE', *, *, #24748, .F. ) ;
#4233=CARTESIAN_POINT ( 'NONE',  ( -46.52287095715007581, -23.48783264082477018, -1.443836473390096797 ) ) ;
#4234=DIRECTION ( 'NONE',  ( -3.773278334444166432E-23, 1.000000000000000000, 0.000000000000000000 ) ) ;
#4235=VECTOR ( 'NONE', #45100, 1000.000000000000114 ) ;
#4236=ORIENTED_EDGE ( 'NONE', *, *, #66303, .T. ) ;
#4238=CARTESIAN_POINT ( 'NONE',  ( 15.69265952521009488, -12.80212094623039576, -1.500000000000002220 ) ) ;
#4239=ADVANCED_FACE ( 'NONE', ( #67791 ), #99997, .T. ) ;
#4240=CARTESIAN_POINT ( 'NONE',  ( -122.5906892859157296, -23.96119346886880663, -0.6495511937832028071 ) ) ;
#4242=CARTESIAN_POINT ( 'NONE',  ( -117.6228709571500559, -29.50248528299804818, 1.056150453629045360 ) ) ;
#4245=EDGE_LOOP ( 'NONE', ( #81772, #48382, #5113, #11906 ) ) ;
#4246=CARTESIAN_POINT ( 'NONE',  ( -78.94303308397304875, -25.27645460285955181, 5.977536667781793156 ) ) ;
#4249=CARTESIAN_POINT ( 'NONE',  ( 12.85705330080557829, 15.37097598829428513, -1.500000000000002220 ) ) ;
#4250=CARTESIAN_POINT ( 'NONE',  ( 8.881738082190086203, 19.07353979602852689, 11.49999999999999645 ) ) ;
#4253=CARTESIAN_POINT ( 'NONE',  ( -19.90388773112789167, 9.559999800501117306, -1.500000000000002220 ) ) ;
#4254=ADVANCED_FACE ( 'NONE', ( #74869 ), #5371, .T. ) ;
#4256=EDGE_CURVE ( 'NONE', #13507, #59016, #5710, .T. ) ;
#4257=CARTESIAN_POINT ( 'NONE',  ( -34.52287095715006160, -23.47593901973090169, -1.443836447538997314 ) ) ;
#4259=ORIENTED_EDGE ( 'NONE', *, *, #66341, .T. ) ;
#4260=FACE_OUTER_BOUND ( 'NONE', #62954, .T. ) ;
#4261=CARTESIAN_POINT ( 'NONE',  ( -31.52200039736317905, -23.48783264082477018, -1.443836473390079256 ) ) ;
#4265=CARTESIAN_POINT ( 'NONE',  ( -72.52287095715007581, -23.48786465467241058, 11.44779295918254647 ) ) ;
#4266=DIRECTION ( 'NONE',  ( -0.000000000000000000, 2.173523156925979552E-06, -0.9999999999976378895 ) ) ;
#4267=CARTESIAN_POINT ( 'NONE',  ( 13.11803791274172681, -15.88952355948706341, -1.500000000000002220 ) ) ;
#4268=CARTESIAN_POINT ( 'NONE',  ( 13.04721882220160012, 17.14300067834640373, 11.49999999999999645 ) ) ;
#4270=DIRECTION ( 'NONE',  ( 0.000000000000000000, -2.173523156925979552E-06, 0.9999999999976378895 ) ) ;
#4274=CARTESIAN_POINT ( 'NONE',  ( -19.39139147909919458, -11.06001032434818576, -1.500000000000002220 ) ) ;
#4275=LINE ( 'NONE', #96123, #38371 ) ;
#4276=DIRECTION ( 'NONE',  ( -3.773278334453079030E-23, 0.9999999999976377785, 2.173523156925979128E-06 ) ) ;
#4277=EDGE_LOOP ( 'NONE', ( #61982, #70823, #62189, #19666 ) ) ;
#4278=CARTESIAN_POINT ( 'NONE',  ( -43.52287095715006160, -24.65952944569304606, 1.056160979905691910 ) ) ;
#4280=CARTESIAN_POINT ( 'NONE',  ( 19.93353245626563819, -6.116835970281883306, 11.49999999999998934 ) ) ;
#4281=EDGE_LOOP ( 'NONE', ( #96717, #61180, #94863, #96240 ) ) ;
#4286=CARTESIAN_POINT ( 'NONE',  ( -100.5441709467755800, -25.00182538069147142, 7.747789668545045139 ) ) ;
#4287=CARTESIAN_POINT ( 'NONE',  ( -13.19772682967519195, -16.48504770976277101, -1.500000000000002220 ) ) ;
#4288=ORIENTED_EDGE ( 'NONE', *, *, #64688, .T. ) ;
#4289=CARTESIAN_POINT ( 'NONE',  ( -114.6228709571500701, -23.47596703998600631, 11.44779298504227860 ) ) ;
#4290=CARTESIAN_POINT ( 'NONE',  ( -49.30576173963486752, -25.30390373665932913, 5.218538515028145142 ) ) ;
#4291=CARTESIAN_POINT ( 'NONE',  ( -120.5543829380116989, -24.40133493613049964, 9.663955038902800609 ) ) ;
#4292=EDGE_CURVE ( 'NONE', #90746, #28117, #65053, .T. ) ;
#4293=CARTESIAN_POINT ( 'NONE',  ( -81.26889613615777819, -25.31615098280113685, 4.442621364743881252 ) ) ;
#4294=DIRECTION ( 'NONE',  ( 0.000000000000000000, -2.173523156925980399E-06, 0.9999999999976378895 ) ) ;
#4295=CARTESIAN_POINT ( 'NONE',  ( -15.83346750871019992, -14.79491179806518630, -1.500000000000002220 ) ) ;
#4296=CARTESIAN_POINT ( 'NONE',  ( -81.47155790579010670, -25.12224225815649348, 6.336855834686440758 ) ) ;
#4297=CARTESIAN_POINT ( 'NONE',  ( 19.02167141253037030, -11.55642654327076535, 11.49999999999999645 ) ) ;
#4299=CARTESIAN_POINT ( 'NONE',  ( -72.62287095715005592, -23.73934037231756733, 11.05740245334329153 ) ) ;
#4309=CARTESIAN_POINT ( 'NONE',  ( -74.62287095715005592, -29.50247984919015209, -1.443849546365055359 ) ) ;
#4313=CARTESIAN_POINT ( 'NONE',  ( -35.52287095715006870, -23.47593901973090169, -1.443836447538997092 ) ) ;
#4315=ORIENTED_EDGE ( 'NONE', *, *, #4133, .F. ) ;
#4316=VECTOR ( 'NONE', #60309, 1000.000000000000114 ) ;
#4317=CARTESIAN_POINT ( 'NONE',  ( -69.52287095715006160, -24.50216790748203977, 0.6166512839542548363 ) ) ;
#4318=CARTESIAN_POINT ( 'NONE',  ( 16.82713599508461400, -14.87465808564757808, -1.500000000000002220 ) ) ;
#4320=EDGE_CURVE ( 'NONE', #19978, #30322, #65055, .T. ) ;
#4322=CARTESIAN_POINT ( 'NONE',  ( -100.2508004467732974, -25.04457302488155079, 7.556254356173342401 ) ) ;
#4323=CARTESIAN_POINT ( 'NONE',  ( -101.6339336904412249, -23.73791477778911485, 11.05961554403170233 ) ) ;
#4325=DIRECTION ( 'NONE',  ( -3.773278334453080206E-23, 0.9999999999976377785, 2.173523156925979975E-06 ) ) ;
#4327=CARTESIAN_POINT ( 'NONE',  ( -130.5728709571501156, -25.30559561715418582, 6.147794833475641596 ) ) ;
#4328=CARTESIAN_POINT ( 'NONE',  ( -11.77723790057865116, -15.68276428244051779, 11.49999999999998934 ) ) ;
#4330=VERTEX_POINT ( 'NONE', #62666 ) ;
#4331=CARTESIAN_POINT ( 'NONE',  ( 7.253797376210795456, 20.28272692992397808, 11.49999999999998934 ) ) ;
#4332=CARTESIAN_POINT ( 'NONE',  ( -75.58953762381671027, -25.00182538069145011, 7.747789668545099317 ) ) ;
#4333=CARTESIAN_POINT ( 'NONE',  ( -81.28341456819592281, -25.31572684435573706, 5.143804157612075656 ) ) ;
#4334=CARTESIAN_POINT ( 'NONE',  ( -81.52287095715006160, -24.64965694238408034, 8.947790433994198267 ) ) ;
#4336=CARTESIAN_POINT ( 'NONE',  ( 7.334040449947802465, -21.76207178258647090, -1.500000000000002220 ) ) ;
#4338=EDGE_CURVE ( 'NONE', #1176, #5085, #10572, .T. ) ;
#4340=PLANE ( 'NONE',  #27263 ) ;
#4341=CARTESIAN_POINT ( 'NONE',  ( -49.54104479505958381, -24.34968618360933590, 0.1864209137778799485 ) ) ;
#4342=CARTESIAN_POINT ( 'NONE',  ( 19.67429046578372365, -4.105084037421226739, 11.49999999999999645 ) ) ;
#4344=CARTESIAN_POINT ( 'NONE',  ( -32.48282705711311280, -24.51419770103159834, 9.386484678747182286 ) ) ;
#4346=CARTESIAN_POINT ( 'NONE',  ( -113.5562042904833788, -23.48783264082479150, -1.443836473390060160 ) ) ;
#4347=B_SPLINE_CURVE_WITH_KNOTS ( 'NONE', 3,
 ( #64406, #55276, #40547, #32928, #31423, #62380, #17698, #23291, #93819, #23801, #54775, #85711, #16190, #47159 ),
 .UNSPECIFIED., .F., .F.,
 ( 4, 2, 2, 2, 2, 2, 4 ),
 ( 0.000000000000000000, 0.0001869308316361848311, 0.0003738616632723696623, 0.0007477233265447393246, 0.001121584989817109041, 0.001308515821453293737, 0.001495446653089478649 ),
 .UNSPECIFIED. ) ;
#4349=CARTESIAN_POINT ( 'NONE',  ( -16.82575997001036328, 10.57904039763333159, -1.500000000000002220 ) ) ;
#4350=EDGE_CURVE ( 'NONE', #29179, #84363, #15406, .T. ) ;
#4351=CARTESIAN_POINT ( 'NONE',  ( -94.52287095715006160, -23.47596703998600631, 11.44779298504228393 ) ) ;
#4352=CARTESIAN_POINT ( 'NONE',  ( -13.19171355488933983, -14.64934158388261665, -1.500000000000002220 ) ) ;
#4357=CARTESIAN_POINT ( 'NONE',  ( -125.6228709571501838, -24.82576562982393398, 8.398263435472967942 ) ) ;
#4359=CARTESIAN_POINT ( 'NONE',  ( 17.37421522561336928, 11.14841987994331696, 11.49999999999999645 ) ) ;
#4362=B_SPLINE_CURVE_WITH_KNOTS ( 'NONE', 3,
 ( #637, #86379, #8758, #61053 ),
 .UNSPECIFIED., .F., .F.,
 ( 4, 4 ),
 ( 0.000000000000000000, 0.0001000000000000028644 ),
 .UNSPECIFIED. ) ;
#4363=CARTESIAN_POINT ( 'NONE',  ( 22.61563695565308407, -1.323143620866313208, 11.49999999999999645 ) ) ;
#4367=CARTESIAN_POINT ( 'NONE',  ( -26.47413879005073056, -24.93063536979281380, 7.801149312106798739 ) ) ;
#4369=ORIENTED_EDGE ( 'NONE', *, *, #65661, .F. ) ;
#4371=ORIENTED_EDGE ( 'NONE', *, *, #32218, .T. ) ;
#4372=EDGE_CURVE ( 'NONE', #43974, #61226, #74714, .T. ) ;
#4373=CARTESIAN_POINT ( 'NONE',  ( -30.57287095715006231, -23.48210175247266562, -1.443836490256470428 ) ) ;
#4374=CARTESIAN_POINT ( 'NONE',  ( -22.32109313027335062, -5.015931025267754251, 11.49999999999998934 ) ) ;
#4375=CARTESIAN_POINT ( 'NONE',  ( -74.62287095715002749, -23.73907113216991860, -1.053371485793227480 ) ) ;
#4376=CARTESIAN_POINT ( 'NONE',  ( -8.857468890034409625, -19.66367526556523870, -1.500000000000002220 ) ) ;
#4377=FACE_OUTER_BOUND ( 'NONE', #481, .T. ) ;
#4378=DIRECTION ( 'NONE',  ( -3.773278334453080206E-23, 0.9999999999976377785, 2.173523156925979975E-06 ) ) ;
#4379=CARTESIAN_POINT ( 'NONE',  ( -19.74168752133572724, 10.86179948771369297, 11.49999999999999645 ) ) ;
#4382=CARTESIAN_POINT ( 'NONE',  ( 19.49364837986538745, 10.19379059548657551, 11.49999999999998934 ) ) ;
#4385=FACE_OUTER_BOUND ( 'NONE', #83513, .T. ) ;
#4386=VERTEX_POINT ( 'NONE', #67041 ) ;
#4387=FACE_OUTER_BOUND ( 'NONE', #33731, .T. ) ;
#4388=CARTESIAN_POINT ( 'NONE',  ( -97.62287095715005592, -29.50250243563736774, 8.947779886222138046 ) ) ;
#4389=ORIENTED_EDGE ( 'NONE', *, *, #95271, .T. ) ;
#4390=VECTOR ( 'NONE', #95261, 1000.000000000000114 ) ;
#4391=FACE_OUTER_BOUND ( 'NONE', #11163, .T. ) ;
#4393=ORIENTED_EDGE ( 'NONE', *, *, #60214, .F. ) ;
#4394=ORIENTED_EDGE ( 'NONE', *, *, #95900, .F. ) ;
#4395=CARTESIAN_POINT ( 'NONE',  ( -80.51244414166535535, -25.03284467579916495, 7.563174216508125269 ) ) ;
#4396=CARTESIAN_POINT ( 'NONE',  ( -89.40841769935767047, -29.50249917535260380, 7.447779886225679213 ) ) ;
#4398=CARTESIAN_POINT ( 'NONE',  ( 16.53694760393551988, -11.94906295602464397, -1.500000000000002220 ) ) ;
#4400=CARTESIAN_POINT ( 'NONE',  ( -71.43540103747046999, -25.13480990690564454, 7.034471417043156372 ) ) ;
#4401=CARTESIAN_POINT ( 'NONE',  ( -29.56144366762476849, -23.65480093107256820, 11.05961561336856391 ) ) ;
#4402=CARTESIAN_POINT ( 'NONE',  ( -97.52287095715006160, -24.64898659630367916, 1.056161002820829697 ) ) ;
#4403=CARTESIAN_POINT ( 'NONE',  ( -70.34543693012690824, -25.03149849800392346, 7.563174219434074530 ) ) ;
#4405=CARTESIAN_POINT ( 'NONE',  ( -28.88251580808842789, -24.76881010668045136, 2.994894255481803658 ) ) ;
#4406=CARTESIAN_POINT ( 'NONE',  ( -87.92287095715005307, -23.47593901973090169, -1.443836447538996870 ) ) ;
#4407=ORIENTED_EDGE ( 'NONE', *, *, #91288, .T. ) ;
#4408=CARTESIAN_POINT ( 'NONE',  ( 5.906898857431191807, -19.90033995357616092, 11.49999999999998934 ) ) ;
#4409=VERTEX_POINT ( 'NONE', #52300 ) ;
#4413=B_SPLINE_CURVE_WITH_KNOTS ( 'NONE', 3,
 ( #79439, #93153, #1332, #63237 ),
 .UNSPECIFIED., .F., .F.,
 ( 4, 4 ),
 ( 0.000000000000000000, 9.999999999997510880E-05 ),
 .UNSPECIFIED. ) ;
#4414=CARTESIAN_POINT ( 'NONE',  ( -90.52380231474226946, -25.23397913219354649, 6.409327625488845825 ) ) ;
#4416=VERTEX_POINT ( 'NONE', #59408 ) ;
#4417=ORIENTED_EDGE ( 'NONE', *, *, #94440, .F. ) ;
#4419=B_SPLINE_CURVE_WITH_KNOTS ( 'NONE', 3,
 ( #54350, #78155, #94400, #17277, #23366, #54851 ),
 .UNSPECIFIED., .F., .F.,
 ( 4, 2, 4 ),
 ( 0.000000000000000000, 0.001380764517854768218, 0.002761529035709536437 ),
 .UNSPECIFIED. ) ;
#4420=CARTESIAN_POINT ( 'NONE',  ( -98.62287095715005592, -23.48786465467241769, 11.44779295918254292 ) ) ;
#4422=CARTESIAN_POINT ( 'NONE',  ( -70.65140973383547873, -25.31201598237044337, 5.348842032383912759 ) ) ;
#4423=CARTESIAN_POINT ( 'NONE',  ( 14.84500176111689207, -16.38379996218902335, 11.49999999999999645 ) ) ;
#4425=CARTESIAN_POINT ( 'NONE',  ( -108.5571772755274651, -23.73766607897671221, -1.055555164236429144 ) ) ;
#4426=CARTESIAN_POINT ( 'NONE',  ( -20.05226876979747530, -10.47825485868949613, -1.500000000000002220 ) ) ;
#4427=EDGE_CURVE ( 'NONE', #52058, #61887, #51736, .T. ) ;
#4428=AXIS2_PLACEMENT_3D ( 'NONE', #41235, #48856, #72190 ) ;
#4429=EDGE_CURVE ( 'NONE', #76857, #4511, #36559, .T. ) ;
#4430=EDGE_CURVE ( 'NONE', #66916, #64607, #3218, .T. ) ;
#4431=CARTESIAN_POINT ( 'NONE',  ( -115.5895802679274595, -24.52399227489127043, 9.353111116836528183 ) ) ;
#4433=ORIENTED_EDGE ( 'NONE', *, *, #64498, .T. ) ;
#4434=EDGE_CURVE ( 'NONE', #14844, #26747, #35909, .T. ) ;
#4435=AXIS2_PLACEMENT_3D ( 'NONE', #8922, #22630, #55111 ) ;
#4437=CARTESIAN_POINT ( 'NONE',  ( -78.62287095715005592, -24.33927499327853994, 9.819080762295810061 ) ) ;
#4439=CARTESIAN_POINT ( 'NONE',  ( -15.68702345270385834, -14.21367052863537417, 11.49999999999998934 ) ) ;
#4441=CARTESIAN_POINT ( 'NONE',  ( -80.62287095715002749, -23.85229601348994777, 10.88205029486208986 ) ) ;
#4442=CARTESIAN_POINT ( 'NONE',  ( -9.338385371603758145, -20.21602636099808237, -1.500000000000002220 ) ) ;
#4443=CARTESIAN_POINT ( 'NONE',  ( -46.62287095715004170, -23.72747288104441665, -1.053458166803663110 ) ) ;
#4444=EDGE_CURVE ( 'NONE', #90864, #27723, #95212, .T. ) ;
#4446=CARTESIAN_POINT ( 'NONE',  ( -66.22287095715007865, -23.47593901973090524, -1.443836447538997980 ) ) ;
#4447=CARTESIAN_POINT ( 'NONE',  ( -104.5895376238167245, -23.47593901973091235, -1.443836447539001089 ) ) ;
#4449=CARTESIAN_POINT ( 'NONE',  ( -103.5228709571500616, -24.50321055353803956, 9.387540953477515160 ) ) ;
#4450=CARTESIAN_POINT ( 'NONE',  ( -44.62287095715004881, -23.47596703998600631, 11.44779298504227505 ) ) ;
#4452=CARTESIAN_POINT ( 'NONE',  ( 9.662506626059768067, -16.94115208737379774, -1.500000000000002220 ) ) ;
#4453=CARTESIAN_POINT ( 'NONE',  ( -9.048234560742015375, 19.43086790383670603, -1.500000000000002220 ) ) ;
#4455=FACE_OUTER_BOUND ( 'NONE', #80543, .T. ) ;
#4456=DIRECTION ( 'NONE',  ( -3.773278334453079618E-23, 0.9999999999976377785, 2.173523156925979975E-06 ) ) ;
#4457=CARTESIAN_POINT ( 'NONE',  ( -22.55118551311790753, 3.560990644294375063, -1.500000000000002220 ) ) ;
#4461=CARTESIAN_POINT ( 'NONE',  ( -106.5222054324230356, -23.48786465467241769, 11.44779295918253403 ) ) ;
#4463=CARTESIAN_POINT ( 'NONE',  ( -3.169371320753151977, 19.67850563098683736, 11.49999999999999645 ) ) ;
#4464=CARTESIAN_POINT ( 'NONE',  ( -104.5495398974881169, -24.51314013834316086, 0.6176544820404171743 ) ) ;
#4466=CARTESIAN_POINT ( 'NONE',  ( -39.62886954152041596, -24.51419770103158413, 9.386484678747189392 ) ) ;
#4467=CARTESIAN_POINT ( 'NONE',  ( -48.64594432017239711, -23.96119346886880663, -0.6495511937831938143 ) ) ;
#4468=ORIENTED_EDGE ( 'NONE', *, *, #27568, .T. ) ;
#4469=CARTESIAN_POINT ( 'NONE',  ( -45.62287095715004881, -29.50247984919015209, -1.443849546365058689 ) ) ;
#4470=CARTESIAN_POINT ( 'NONE',  ( -31.21619930677465504, -25.31600595412499644, 6.101236642668423471 ) ) ;
#4472=CARTESIAN_POINT ( 'NONE',  ( -10.76533847658563126, -18.86179312034942868, 11.49999999999998934 ) ) ;
#4474=CARTESIAN_POINT ( 'NONE',  ( -0.4769873229303308038, -19.55164744950295841, -1.500000000000002220 ) ) ;
#4475=CARTESIAN_POINT ( 'NONE',  ( -55.55110250455299337, -24.15602025860896518, 10.28564288303535257 ) ) ;
#4479=CARTESIAN_POINT ( 'NONE',  ( -89.62287095715004170, -23.47596703998600631, 11.44779298504227860 ) ) ;
#4480=CARTESIAN_POINT ( 'NONE',  ( -16.87313589883980214, -11.49665204554024989, 11.49999999999999645 ) ) ;
#4483=ORIENTED_EDGE ( 'NONE', *, *, #8647, .T. ) ;
#4484=CARTESIAN_POINT ( 'NONE',  ( -53.52287095715006870, -23.47596703998600631, 11.44779298504229104 ) ) ;
#4488=CARTESIAN_POINT ( 'NONE',  ( -67.52287095715006160, -23.47596703998600631, 11.44779298504228748 ) ) ;
#4491=VECTOR ( 'NONE', #13376, 1000.000000000000114 ) ;
#4492=CARTESIAN_POINT ( 'NONE',  ( 22.26416322464526232, -5.798680748638591176, 11.49999999999999645 ) ) ;
#4493=CARTESIAN_POINT ( 'NONE',  ( -22.77908990650604792, -0.06651829912971220227, -1.500000000000002220 ) ) ;
#4494=CARTESIAN_POINT ( 'NONE',  ( -110.5103923454349939, -25.00182538069147142, 7.747789668545045139 ) ) ;
#4495=B_SPLINE_CURVE_WITH_KNOTS ( 'NONE', 3,
 ( #76729, #53431, #36698, #53929, #21946, #52931 ),
 .UNSPECIFIED., .F., .F.,
 ( 4, 2, 4 ),
 ( 0.000000000000000000, 0.001380901958385385509, 0.002761803916770771018 ),
 .UNSPECIFIED. ) ;
#4496=B_SPLINE_SURFACE_WITH_KNOTS ( 'NONE', 3, 3, ( 
 ( #37821, #61675, #23070, #14469 ),
 ( #69269, #76856, #100185, #13975 ),
 ( #76365, #37334, #46430, #7863 ),
 ( #68278, #45451, #54060, #77361 ),
 ( #30704, #91105, #38809, #99208 ),
 ( #83487, #70268, #14972, #61179 ),
 ( #93092, #15965, #21580, #53563 ) ),
 .UNSPECIFIED., .F., .F., .F.,
 ( 4, 3, 4 ),
 ( 4, 4 ),
 ( 0.7945040050992246972, 0.8970133687736505657, 0.9995227324480763231 ),
 ( 0.5796412921291099751, 0.5809216175690411488 ),
 .UNSPECIFIED. ) ;
#4497=CARTESIAN_POINT ( 'NONE',  ( -36.62287095715005592, -29.50250786944525672, 11.44777988621624232 ) ) ;
#4499=CARTESIAN_POINT ( 'NONE',  ( -70.52287095715007581, -24.15431212366388891, -0.2830839119429260364 ) ) ;
#4500=CARTESIAN_POINT ( 'NONE',  ( -110.5975878789654274, -23.48783264082476663, -1.443836473390091690 ) ) ;
#4501=CARTESIAN_POINT ( 'NONE',  ( -21.08706934527708654, 5.832127334627817739, 11.49999999999998934 ) ) ;
#4504=CARTESIAN_POINT ( 'NONE',  ( -120.6228709571500701, -24.82558206586149652, 1.605769216559631341 ) ) ;
#4505=CARTESIAN_POINT ( 'NONE',  ( -58.53812816766490101, -24.51314013834315020, 0.6176544820404091807 ) ) ;
#4506=ORIENTED_EDGE ( 'NONE', *, *, #100335, .F. ) ;
#4507=CARTESIAN_POINT ( 'NONE',  ( 3.609400094169940676, -20.08663944828865766, -1.500000000000002220 ) ) ;
#4508=ORIENTED_EDGE ( 'NONE', *, *, #71674, .T. ) ;
#4509=ORIENTED_EDGE ( 'NONE', *, *, #62263, .F. ) ;
#4510=ORIENTED_EDGE ( 'NONE', *, *, #33159, .T. ) ;
#4511=VERTEX_POINT ( 'NONE', #19342 ) ;
#4512=CARTESIAN_POINT ( 'NONE',  ( 22.92345266703080142, -2.467471440992916154, -1.500000000000002220 ) ) ;
#4513=CARTESIAN_POINT ( 'NONE',  ( -80.52287095715006160, -25.00158670708909625, 2.256160236439166411 ) ) ;
#4514=CARTESIAN_POINT ( 'NONE',  ( 11.17094659993960803, -16.83544227557131023, -1.500000000000002220 ) ) ;
#4515=ORIENTED_EDGE ( 'NONE', *, *, #29755, .T. ) ;
#4516=CARTESIAN_POINT ( 'NONE',  ( -98.62287095715005592, -24.64965695001469115, 8.947790433994178727 ) ) ;
#4518=CARTESIAN_POINT ( 'NONE',  ( -34.52287095715006160, -24.64965694238575011, 8.947790433994207149 ) ) ;
#4520=CARTESIAN_POINT ( 'NONE',  ( -53.50784545873391096, -23.96169478059712787, 10.65365249895718591 ) ) ;
#4521=CARTESIAN_POINT ( 'NONE',  ( 2.027878592902508270, 21.29203748114955985, 11.49999999999999645 ) ) ;
#4522=ORIENTED_EDGE ( 'NONE', *, *, #6230, .T. ) ;
#4523=CARTESIAN_POINT ( 'NONE',  ( 6.026614999332422182E-17, -23.47593901973084485, -1.443836476861628304 ) ) ;
#4524=ORIENTED_EDGE ( 'NONE', *, *, #89345, .F. ) ;
#4525=CARTESIAN_POINT ( 'NONE',  ( 2.321567282091853812, -22.14299765706108403, -1.500000000000002220 ) ) ;
#4526=CARTESIAN_POINT ( 'NONE',  ( -13.01863806243235899, 16.06808769575019014, -1.500000000000002220 ) ) ;
#4527=AXIS2_PLACEMENT_3D ( 'NONE', #90989, #13859, #52439 ) ;
#4528=VERTEX_POINT ( 'NONE', #96468 ) ;
#4529=CARTESIAN_POINT ( 'NONE',  ( -55.62287095715005592, -29.50250786944525672, 11.44777988621623876 ) ) ;
#4531=EDGE_CURVE ( 'NONE', #98739, #60599, #51298, .T. ) ;
#4532=CARTESIAN_POINT ( 'NONE',  ( -81.52287095715009002, -23.73907113217678955, -1.053371485781112282 ) ) ;
#4534=ORIENTED_EDGE ( 'NONE', *, *, #96856, .T. ) ;
#4536=EDGE_CURVE ( 'NONE', #75736, #27742, #82735, .T. ) ;
#4537=CARTESIAN_POINT ( 'NONE',  ( 15.12549221760053086, 14.48511125727034177, -1.500000000000002220 ) ) ;
#4538=CARTESIAN_POINT ( 'NONE',  ( -16.24880213243413607, 14.73142910551002238, 11.49999999999999645 ) ) ;
#4541=CARTESIAN_POINT ( 'NONE',  ( -15.68175098440391402, -16.16561365185589594, -1.500000000000002220 ) ) ;
#4543=CARTESIAN_POINT ( 'NONE',  ( 0.8316226063609513108, 20.92010288561657205, 11.49999999999998934 ) ) ;
#4544=CARTESIAN_POINT ( 'NONE',  ( -89.40841769935767047, -25.11033443737731474, 2.832404817301930056 ) ) ;
#4546=EDGE_CURVE ( 'NONE', #32133, #11978, #72217, .T. ) ;
#4547=CARTESIAN_POINT ( 'NONE',  ( -119.5556264641217723, -23.96169478059714564, 10.65365249895717170 ) ) ;
#4549=ORIENTED_EDGE ( 'NONE', *, *, #32492, .F. ) ;
#4550=ORIENTED_EDGE ( 'NONE', *, *, #12541, .F. ) ;
#4554=CARTESIAN_POINT ( 'NONE',  ( 9.988417798295188277, 18.97302403871600518, -1.500000000000002220 ) ) ;
#4556=ORIENTED_EDGE ( 'NONE', *, *, #97384, .F. ) ;
#4557=CARTESIAN_POINT ( 'NONE',  ( -16.00611555608923098, 13.71732778110762219, 11.49999999999998934 ) ) ;
#4558=CARTESIAN_POINT ( 'NONE',  ( -100.2210274182397711, -25.19675915012271616, 3.305962695313816813 ) ) ;
#4560=CARTESIAN_POINT ( 'NONE',  ( -87.62287095715009855, -24.34917612406837506, 0.1852690917426670081 ) ) ;
#4562=CARTESIAN_POINT ( 'NONE',  ( -100.5228709571500616, -24.99132157543084531, 2.256160258750667502 ) ) ;
#4563=CARTESIAN_POINT ( 'NONE',  ( 6.025212951983072607, -21.27585971943098642, -1.500000000000002220 ) ) ;
#4564=CARTESIAN_POINT ( 'NONE',  ( -110.2929128916653525, -25.14264220134206695, 6.986250900936242125 ) ) ;
#4566=CARTESIAN_POINT ( 'NONE',  ( -63.55620429048337883, -23.47593901973091235, -1.443836447539007972 ) ) ;
#4567=B_SPLINE_CURVE_WITH_KNOTS ( 'NONE', 3,
 ( #37542, #99428, #68001, #97443 ),
 .UNSPECIFIED., .F., .F.,
 ( 4, 4 ),
 ( 0.000000000000000000, 1.000000000000000000 ),
 .UNSPECIFIED. ) ;
#4568=CARTESIAN_POINT ( 'NONE',  ( -62.63696707577763334, -24.15620529776627379, 10.23563542870660825 ) ) ;
#4570=VERTEX_POINT ( 'NONE', #29444 ) ;
#4572=CARTESIAN_POINT ( 'NONE',  ( 7.684279652734260502, -19.92951104315265809, -1.500000000000002220 ) ) ;
#4573=CARTESIAN_POINT ( 'NONE',  ( -76.52287095715007581, -29.50248528299804818, 1.056150453629038477 ) ) ;
#4574=CARTESIAN_POINT ( 'NONE',  ( -49.88696936683380301, -25.25978491487771649, 3.590542621692356384 ) ) ;
#4575=CARTESIAN_POINT ( 'NONE',  ( -64.54879172121601982, -24.15620529776628445, 10.23563542870660115 ) ) ;
#4576=CARTESIAN_POINT ( 'NONE',  ( -68.55620429048339304, -23.48783264082478084, -1.443836473390067265 ) ) ;
#4577=CARTESIAN_POINT ( 'NONE',  ( 18.79633983808273712, -12.56333175589740847, -1.500000000000002220 ) ) ;
#4578=B_SPLINE_SURFACE_WITH_KNOTS ( 'NONE', 3, 3, ( 
 ( #38424, #31309, #62278, #23688 ),
 ( #54662, #16080, #47050, #70378 ),
 ( #87608, #70889, #72390, #87098 ),
 ( #39926, #47552, #78473, #71388 ),
 ( #1380, #8973, #31820, #80484 ),
 ( #48048, #62789, #49056, #93704 ),
 ( #2375, #86598, #78978, #57177 ) ),
 .UNSPECIFIED., .F., .F., .F.,
 ( 4, 3, 4 ),
 ( 4, 4 ),
 ( 0.0004766839783820824798, 0.1029713700210898031, 0.2054660560637975308 ),
 ( 0.3395803806953949788, 0.3407497870151264818 ),
 .UNSPECIFIED. ) ;
#4579=DIRECTION ( 'NONE',  ( 0.000000000000000000, 0.9999999999976377785, 2.173523156925979975E-06 ) ) ;
#4582=DIRECTION ( 'NONE',  ( -3.773278334453079618E-23, 0.9999999999976377785, 2.173523156925979975E-06 ) ) ;
#4583=CARTESIAN_POINT ( 'NONE',  ( 16.04393857186779115, -11.51807295290239885, 11.49999999999999645 ) ) ;
#4585=CARTESIAN_POINT ( 'NONE',  ( -67.59731535907285149, -23.96119346886880308, -0.6495511937832114668 ) ) ;
#4586=VERTEX_POINT ( 'NONE', #75609 ) ;
#4588=CARTESIAN_POINT ( 'NONE',  ( -29.74701180552300883, -24.60094371313986983, 3.841292727239494109 ) ) ;
#4589=CARTESIAN_POINT ( 'NONE',  ( -101.1692196971220312, -25.17353295164373250, 6.877671026811838395 ) ) ;
#4590=CARTESIAN_POINT ( 'NONE',  ( 14.26105141482337935, -16.23293960606763520, -1.500000000000002220 ) ) ;
#4591=CARTESIAN_POINT ( 'NONE',  ( -49.10457154551148307, -25.27518131127733270, 3.999772247467727304 ) ) ;
#4593=CARTESIAN_POINT ( 'NONE',  ( 11.20917403917954225, 15.81763734437701885, -1.500000000000002220 ) ) ;
#4595=CARTESIAN_POINT ( 'NONE',  ( -97.55620429048340725, -23.47596703998600631, 11.44779298504227683 ) ) ;
#4596=ADVANCED_FACE ( 'NONE', ( #45190 ), #44924, .T. ) ;
#4597=CARTESIAN_POINT ( 'NONE',  ( 16.35176858736616978, 11.14859404531058473, 11.49999999999998934 ) ) ;
#4598=ORIENTED_EDGE ( 'NONE', *, *, #8683, .F. ) ;
#4599=CARTESIAN_POINT ( 'NONE',  ( 19.34776771173714849, 6.126202725962671458, 11.49999999999999645 ) ) ;
#4602=AXIS2_PLACEMENT_3D ( 'NONE', #24858, #32478, #9135 ) ;
#4604=ORIENTED_EDGE ( 'NONE', *, *, #83320, .T. ) ;
#4605=DIRECTION ( 'NONE',  ( -1.000000000000000000, -3.773278334444167608E-23, -8.201307833595939069E-29 ) ) ;
#4606=CARTESIAN_POINT ( 'NONE',  ( -108.8968792378191921, -25.06732983082694943, 7.447789526168955732 ) ) ;
#4607=CARTESIAN_POINT ( 'NONE',  ( -123.5228709571500616, -29.50247984919015209, -1.443849546365046699 ) ) ;
#4609=CARTESIAN_POINT ( 'NONE',  ( -95.62287095715002749, -23.85196035786901092, -0.8779234886474903687 ) ) ;
#4610=B_SPLINE_CURVE_WITH_KNOTS ( 'NONE', 3,
 ( #31848, #87636, #62816, #10500 ),
 .UNSPECIFIED., .F., .F.,
 ( 4, 4 ),
 ( 0.8203717318505863165, 0.8293781631227020723 ),
 .UNSPECIFIED. ) ;
#4611=LINE ( 'NONE', #89833, #86767 ) ;
#4612=CARTESIAN_POINT ( 'NONE',  ( 7.608091486120485136, 18.53616061196756704, -1.500000000000002220 ) ) ;
#4615=CARTESIAN_POINT ( 'NONE',  ( -32.62287095715004170, -23.73934037231755667, 11.05740245334329508 ) ) ;
#4617=CARTESIAN_POINT ( 'NONE',  ( -76.62287095715007013, -29.50247984919015209, -1.443849546365053582 ) ) ;
#4620=CARTESIAN_POINT ( 'NONE',  ( -50.78612140924919771, -25.12100811749006724, 7.112893600995336740 ) ) ;
#4621=ORIENTED_EDGE ( 'NONE', *, *, #5912, .T. ) ;
#4622=CARTESIAN_POINT ( 'NONE',  ( -20.07547297788957152, 3.163885811906596679, -1.500000000000002220 ) ) ;
#4623=EDGE_LOOP ( 'NONE', ( #59326, #40610, #84625, #66666 ) ) ;
#4624=CARTESIAN_POINT ( 'NONE',  ( 2.319610639010541764, -22.79860127089448696, -1.500000000000002220 ) ) ;
#4627=CARTESIAN_POINT ( 'NONE',  ( -49.74369414166532266, -25.30543060587212167, 4.940877950953177944 ) ) ;
#4628=CARTESIAN_POINT ( 'NONE',  ( -50.16062266432883376, -25.26264174977159271, 7.085347539999360400 ) ) ;
#4629=CARTESIAN_POINT ( 'NONE',  ( -117.5228709571500758, -23.48786465467241769, 11.44779295918253759 ) ) ;
#4630=CARTESIAN_POINT ( 'NONE',  ( -6.347832186973104029, -20.24257907634199682, 11.49999999999999645 ) ) ;
#4632=CARTESIAN_POINT ( 'NONE',  ( -21.91529987491217923, -3.391794311424265018, 11.49999999999998934 ) ) ;
#4633=B_SPLINE_CURVE_WITH_KNOTS ( 'NONE', 3,
 ( #42536, #42036, #73968, #43524 ),
 .UNSPECIFIED., .F., .F.,
 ( 4, 4 ),
 ( 0.000000000000000000, 9.999999999993348899E-05 ),
 .UNSPECIFIED. ) ;
#4634=CARTESIAN_POINT ( 'NONE',  ( 10.47388184937329214, 17.72644800832989986, -1.500000000000002220 ) ) ;
#4636=ORIENTED_EDGE ( 'NONE', *, *, #56225, .F. ) ;
#4638=CARTESIAN_POINT ( 'NONE',  ( -50.52287095715006160, -24.99156044556120193, 7.747789690856173195 ) ) ;
#4639=ORIENTED_EDGE ( 'NONE', *, *, #25265, .T. ) ;
#4640=EDGE_CURVE ( 'NONE', #30940, #24715, #37163, .T. ) ;
#4641=ORIENTED_EDGE ( 'NONE', *, *, #88047, .F. ) ;
#4642=EDGE_LOOP ( 'NONE', ( #58103, #79505, #82496, #6564, #64310, #12909, #4407, #15201 ) ) ;
#4644=CARTESIAN_POINT ( 'NONE',  ( -28.50259040100463181, -23.79745624473767762, 10.65365253163527193 ) ) ;
#4646=CARTESIAN_POINT ( 'NONE',  ( 19.63682106917175929, 6.691539877478525966, -1.500000000000002220 ) ) ;
#4647=CARTESIAN_POINT ( 'NONE',  ( 5.343276940429747768, -21.04383479052346217, 11.49999999999999645 ) ) ;
#4648=VERTEX_POINT ( 'NONE', #76115 ) ;
#4649=EDGE_CURVE ( 'NONE', #73442, #420, #55332, .T. ) ;
#4650=CARTESIAN_POINT ( 'NONE',  ( -70.62287095715005592, -24.99156045073392463, 7.747789690856161648 ) ) ;
#4651=CARTESIAN_POINT ( 'NONE',  ( -119.6228709571500417, -24.66019654487199730, 8.947790411086121054 ) ) ;
#4652=CARTESIAN_POINT ( 'NONE',  ( 21.09243369641204069, 7.689775423913054908, 11.49999999999998934 ) ) ;
#4653=VECTOR ( 'NONE', #58754, 1000.000000000000114 ) ;
#4654=EDGE_CURVE ( 'NONE', #36107, #17029, #8046, .T. ) ;
#4656=CARTESIAN_POINT ( 'NONE',  ( -34.92287095715006018, -23.47596703998600276, 11.44779298504227683 ) ) ;
#4658=CARTESIAN_POINT ( 'NONE',  ( -98.52287095715006160, -23.47596703998600631, 11.44779298504228215 ) ) ;
#4659=CARTESIAN_POINT ( 'NONE',  ( -41.46611000704998418, -25.27828342519987359, 4.188173683033348915 ) ) ;
#4663=ORIENTED_EDGE ( 'NONE', *, *, #74985, .F. ) ;
#4664=CARTESIAN_POINT ( 'NONE',  ( -46.64014493302430253, -24.15620529776627379, 10.23563542870660825 ) ) ;
#4666=CARTESIAN_POINT ( 'NONE',  ( 17.95810460983813783, 11.44545274529666479, -1.500000000000002220 ) ) ;
#4667=EDGE_LOOP ( 'NONE', ( #64096, #75030, #66816, #87741 ) ) ;
#4668=PLANE ( 'NONE',  #8947 ) ;
#4669=CARTESIAN_POINT ( 'NONE',  ( 8.107222467604051630, 20.28165043084963060, -1.500000000000002220 ) ) ;
#4671=CARTESIAN_POINT ( 'NONE',  ( -1.179572987637725889, 22.66035800735570049, 11.49999999999998934 ) ) ;
#4673=CARTESIAN_POINT ( 'NONE',  ( -40.55984193903805846, -25.18430871972357465, 3.296901506826879658 ) ) ;
#4675=CARTESIAN_POINT ( 'NONE',  ( 6.821863743248424150, 20.85434273413645911, -1.500000000000002220 ) ) ;
#4680=CARTESIAN_POINT ( 'NONE',  ( -110.3346797185884327, -29.50249014687182836, 3.293933732389337621 ) ) ;
#4681=ORIENTED_EDGE ( 'NONE', *, *, #40955, .F. ) ;
#4682=CARTESIAN_POINT ( 'NONE',  ( -30.60135620917391108, -24.67298148219492759, 8.885272145915891429 ) ) ;
#4683=B_SPLINE_CURVE_WITH_KNOTS ( 'NONE', 3,
 ( #73401, #43941, #82985, #44447, #74874, #67796 ),
 .UNSPECIFIED., .F., .F.,
 ( 4, 2, 4 ),
 ( 6.389872268825926790E-06, 0.001387607747329055096, 0.002768825622389284574 ),
 .UNSPECIFIED. ) ;
#4684=CARTESIAN_POINT ( 'NONE',  ( -128.5228709571500758, -23.47596703998600631, 11.44779298504227683 ) ) ;
#4685=CARTESIAN_POINT ( 'NONE',  ( -30.62897883088349005, -24.04641872041738893, -0.4716817114508958242 ) ) ;
#4686=CARTESIAN_POINT ( 'NONE',  ( 4.782327729912362990, -20.71560727227588927, 11.49999999999998934 ) ) ;
#4687=CARTESIAN_POINT ( 'NONE',  ( -112.5880318784174534, -24.51314013834317151, 0.6176544820404282765 ) ) ;
#4688=CARTESIAN_POINT ( 'NONE',  ( -26.09735693242928534, -24.75186533036128367, 4.864566394564080021 ) ) ;
#4690=CARTESIAN_POINT ( 'NONE',  ( -129.5228709571499905, -23.48783264082477729, -1.443836473390079700 ) ) ;
#4691=DIRECTION ( 'NONE',  ( -3.773278334453080206E-23, 0.9999999999976377785, 2.173523156925979975E-06 ) ) ;
#4692=ORIENTED_EDGE ( 'NONE', *, *, #61961, .F. ) ;
#4693=CARTESIAN_POINT ( 'NONE',  ( 14.99095386781537975, 12.61000069877385421, 11.49999999999999645 ) ) ;
#4694=CARTESIAN_POINT ( 'NONE',  ( -42.92287095715004597, -23.47593901973090169, -1.443836447538997980 ) ) ;
#4695=CARTESIAN_POINT ( 'NONE',  ( -28.42960646346242015, -24.73443543797376520, 8.111062014341033688 ) ) ;
#4696=EDGE_CURVE ( 'NONE', #98343, #60391, #45621, .T. ) ;
#4699=CARTESIAN_POINT ( 'NONE',  ( -99.30030995969208618, -25.31470181650071183, 5.154044150389992751 ) ) ;
#4700=DIRECTION ( 'NONE',  ( 0.000000000000000000, -2.173523156925979552E-06, 0.9999999999976378895 ) ) ;
#4702=CARTESIAN_POINT ( 'NONE',  ( 5.252985061998082017, 18.97096265210048571, -1.500000000000002220 ) ) ;
#4710=CARTESIAN_POINT ( 'NONE',  ( -45.62287095715004881, -24.83620972994591725, 8.398175272781360334 ) ) ;
#4711=FACE_OUTER_BOUND ( 'NONE', #67913, .T. ) ;
#4712=CARTESIAN_POINT ( 'NONE',  ( -84.55620429048340725, -23.47596703998600631, 11.44779298504227683 ) ) ;
#4713=FACE_OUTER_BOUND ( 'NONE', #66376, .T. ) ;
#4716=CARTESIAN_POINT ( 'NONE',  ( -128.6228709571500417, -29.50247984919015209, -1.443849546365044922 ) ) ;
#4717=CARTESIAN_POINT ( 'NONE',  ( -107.5944960464543243, -23.73766607897672642, -1.055555164236427590 ) ) ;
#4718=CARTESIAN_POINT ( 'NONE',  ( 1.593314845114734535, -19.89410510517485164, -1.500000000000002220 ) ) ;
#4721=CARTESIAN_POINT ( 'NONE',  ( -0.07405751743314503699, -22.09126723942814863, 0.2209411766731599891 ) ) ;
#4727=CARTESIAN_POINT ( 'NONE',  ( -124.6622648968966871, -25.28354030677812148, 5.756449734795270778 ) ) ;
#4728=CARTESIAN_POINT ( 'NONE',  ( -81.63689468831775287, -23.96119346886881019, -0.6495511937831893734 ) ) ;
#4729=VECTOR ( 'NONE', #35434, 1000.000000000000000 ) ;
#4730=CARTESIAN_POINT ( 'NONE',  ( -26.09825697877282735, -24.96875754738233866, 4.795748209963784703 ) ) ;
#4732=CARTESIAN_POINT ( 'NONE',  ( -88.62287095715004170, -24.64898659630367916, 1.056161002820827921 ) ) ;
#4736=ORIENTED_EDGE ( 'NONE', *, *, #24661, .T. ) ;
#4738=CARTESIAN_POINT ( 'NONE',  ( -9.806399893892750796, 17.69452640759178408, -1.500000000000002220 ) ) ;
#4742=ORIENTED_EDGE ( 'NONE', *, *, #80825, .F. ) ;
#4743=CARTESIAN_POINT ( 'NONE',  ( -78.97891443407796430, -25.30125878307690357, 5.600169338922809104 ) ) ;
#4744=DIRECTION ( 'NONE',  ( 0.000000000000000000, -0.9999999999976377785, -2.173523156925979128E-06 ) ) ;
#4745=CARTESIAN_POINT ( 'NONE',  ( -10.42242239376218116, -17.14354752861867937, -1.500000000000002220 ) ) ;
#4746=CARTESIAN_POINT ( 'NONE',  ( -2.129267666952235682, 20.92775224702969439, 11.49999999999999645 ) ) ;
#4747=CARTESIAN_POINT ( 'NONE',  ( -116.4728709571500360, -25.40558663563427189, 5.000950442582703381 ) ) ;
#4748=CARTESIAN_POINT ( 'NONE',  ( -70.57978950566615595, -24.92592662359561118, 8.075495903017998245 ) ) ;
#4749=CARTESIAN_POINT ( 'NONE',  ( -16.08457400211760913, 15.13120210334024662, -1.500000000000002220 ) ) ;
#4750=CARTESIAN_POINT ( 'NONE',  ( -40.31138024738270786, -25.31589329286174817, 5.079523608772094967 ) ) ;
#4751=CARTESIAN_POINT ( 'NONE',  ( -71.30457154551150722, -25.25559839591754496, 6.209207386190694677 ) ) ;
#4752=CARTESIAN_POINT ( 'NONE',  ( -50.40445135320380388, -25.27344759577556843, 3.293942924311254572 ) ) ;
#4753=ORIENTED_EDGE ( 'NONE', *, *, #88211, .F. ) ;
#4754=CARTESIAN_POINT ( 'NONE',  ( -89.81226385320383088, -29.50249691823240994, 6.409318347766594037 ) ) ;
#4755=B_SPLINE_SURFACE_WITH_KNOTS ( 'NONE', 3, 3, ( 
 ( #62778, #31299, #62266, #96212 ),
 ( #33297, #64789, #33807, #10970 ),
 ( #25183, #80978, #42439, #17577 ),
 ( #88103, #40423, #48549, #18572 ),
 ( #57165, #49047, #65782, #25690 ),
 ( #88599, #9967, #71380, #49546 ),
 ( #56160, #19071, #57657, #64283 ) ),
 .UNSPECIFIED., .F., .F., .F.,
 ( 4, 3, 4 ),
 ( 4, 4 ),
 ( 0.0004766839783822500432, 0.1029713700210897753, 0.2054660560637973088 ),
 ( 0.3295778362189659139, 0.3307426273830550989 ),
 .UNSPECIFIED. ) ;
#4756=CARTESIAN_POINT ( 'NONE',  ( -31.62287095715006657, -24.34917612406837506, 0.1852690917426561001 ) ) ;
#4758=ORIENTED_EDGE ( 'NONE', *, *, #13788, .F. ) ;
#4759=DIRECTION ( 'NONE',  ( -0.000000000000000000, 2.173523156925979552E-06, -0.9999999999976378895 ) ) ;
#4761=CARTESIAN_POINT ( 'NONE',  ( -89.62287095714999907, -23.96127896941631619, -0.6493128931037825957 ) ) ;
#4762=CARTESIAN_POINT ( 'NONE',  ( -19.39287000742378453, 6.875061630626206011, -1.500000000000002220 ) ) ;
#4763=CARTESIAN_POINT ( 'NONE',  ( -21.33164055427280914, -3.227942221655450972, 11.49999999999999645 ) ) ;
#4767=CARTESIAN_POINT ( 'NONE',  ( -97.52287095715010423, -23.48783264082477018, -1.443836473390087027 ) ) ;
#4768=CARTESIAN_POINT ( 'NONE',  ( 20.23429811176546167, 9.490607074118958764, -1.500000000000002220 ) ) ;
#4771=ORIENTED_EDGE ( 'NONE', *, *, #23500, .T. ) ;
#4773=CARTESIAN_POINT ( 'NONE',  ( -51.66770628948501098, -25.28171047118814840, 4.239413304054294507 ) ) ;
#4775=CARTESIAN_POINT ( 'NONE',  ( 16.07097863352054290, 13.35096362007907622, 11.49999999999998934 ) ) ;
#4776=EDGE_CURVE ( 'NONE', #60884, #63331, #22581, .T. ) ;
#4778=CARTESIAN_POINT ( 'NONE',  ( -92.55620429048339304, -24.65952944569304606, 1.056160979905701680 ) ) ;
#4781=CARTESIAN_POINT ( 'NONE',  ( -100.5540350906619409, -24.15602025860896163, 10.28564288303535790 ) ) ;
#4782=CARTESIAN_POINT ( 'NONE',  ( -18.69274626484788371, 9.848020819832786543, -1.500000000000002220 ) ) ;
#4784=CARTESIAN_POINT ( 'NONE',  ( -91.52287095715010423, -24.66019654487199730, 8.947790411086115725 ) ) ;
#4785=CARTESIAN_POINT ( 'NONE',  ( -102.6228709571500275, -23.95044443724990657, 10.65354141964649592 ) ) ;
#4786=CARTESIAN_POINT ( 'NONE',  ( -61.52287095715006160, -23.48786465467241058, 11.44779295918254824 ) ) ;
#4788=CARTESIAN_POINT ( 'NONE',  ( -76.54257616626556171, -24.51419770103157347, 9.386484678747176957 ) ) ;
#4790=CARTESIAN_POINT ( 'NONE',  ( -21.76810506448615712, 0.6044244127108716613, -1.500000000000002220 ) ) ;
#4791=CARTESIAN_POINT ( 'NONE',  ( -80.83723253079826065, -25.24759792921647872, 7.046395315168356710 ) ) ;
#4792=CARTESIAN_POINT ( 'NONE',  ( 22.20884612314100792, -2.053178116692622623, 11.49999999999999645 ) ) ;
#4793=ORIENTED_EDGE ( 'NONE', *, *, #4654, .T. ) ;
#4794=ADVANCED_FACE ( 'NONE', ( #32966 ), #29504, .T. ) ;
#4797=CARTESIAN_POINT ( 'NONE',  ( -36.62287095715005592, -23.48786465467240347, 11.44779295918255180 ) ) ;
#4800=CARTESIAN_POINT ( 'NONE',  ( -40.62287095715005592, -23.48783264082478084, -1.443836473390072817 ) ) ;
#4801=ORIENTED_EDGE ( 'NONE', *, *, #57917, .F. ) ;
#4802=AXIS2_PLACEMENT_3D ( 'NONE', #74244, #96092, #57543 ) ;
#4803=ORIENTED_EDGE ( 'NONE', *, *, #40787, .F. ) ;
#4805=CARTESIAN_POINT ( 'NONE',  ( -95.58953762381672448, -24.99156044556120193, 7.747789690856343725 ) ) ;
#4806=CARTESIAN_POINT ( 'NONE',  ( -86.55620429048336462, -23.47596703998600631, 11.44779298504227683 ) ) ;
#4807=CARTESIAN_POINT ( 'NONE',  ( -49.65643811812167741, -25.31518051169904027, 4.891465044530135309 ) ) ;
#4808=VECTOR ( 'NONE', #62200, 1000.000000000000114 ) ;
#4809=CARTESIAN_POINT ( 'NONE',  ( -35.52287095715006870, -24.91544648472619627, 1.928969306349232582 ) ) ;
#4810=CARTESIAN_POINT ( 'NONE',  ( -66.52287095715006160, -23.47596703998600631, 11.44779298504228748 ) ) ;
#4812=CARTESIAN_POINT ( 'NONE',  ( -18.22047185089115828, 6.579378235550767506, 11.49999999999999645 ) ) ;
#4817=CARTESIAN_POINT ( 'NONE',  ( -102.6228709571500133, -23.96127896941632685, -0.6493128931037813745 ) ) ;
#4818=CARTESIAN_POINT ( 'NONE',  ( -48.52287095715006160, -29.50250243563736774, 8.947779886222146928 ) ) ;
#4819=EDGE_CURVE ( 'NONE', #65087, #69040, #26198, .T. ) ;
#4820=CARTESIAN_POINT ( 'NONE',  ( -15.04504930077994196, -12.58455232801425794, -1.500000000000002220 ) ) ;
#4821=CARTESIAN_POINT ( 'NONE',  ( -116.5228709571500616, -24.65952944569305316, 1.056160979905705899 ) ) ;
#4822=EDGE_LOOP ( 'NONE', ( #40471, #35218, #4197, #47443 ) ) ;
#4823=CARTESIAN_POINT ( 'NONE',  ( -7.189238790567602067, -20.27908067168375794, 11.49999999999998934 ) ) ;
#4825=CARTESIAN_POINT ( 'NONE',  ( -81.28341456819592281, -25.30394797635934978, 5.143804183213717351 ) ) ;
#4826=CARTESIAN_POINT ( 'NONE',  ( -40.67672227337696000, -23.48783264082477018, -1.443836473390102570 ) ) ;
#4828=CARTESIAN_POINT ( 'NONE',  ( -5.582908757718670678, 22.30220962497079285, -1.500000000000002220 ) ) ;
#4829=ADVANCED_FACE ( 'NONE', ( #26848 ), #58311, .F. ) ;
#4833=CARTESIAN_POINT ( 'NONE',  ( -18.21026628907936029, 8.684577975296603469, 11.49999999999999645 ) ) ;
#4834=CARTESIAN_POINT ( 'NONE',  ( -101.6228709571500559, -24.64898659630368627, 1.056161002820829697 ) ) ;
#4839=CARTESIAN_POINT ( 'NONE',  ( -19.55781625546462976, 3.520333346782119843, -1.500000000000002220 ) ) ;
#4840=CARTESIAN_POINT ( 'NONE',  ( -113.5917735524323575, -23.96119346886881374, -0.6495511937832029181 ) ) ;
#4841=CARTESIAN_POINT ( 'NONE',  ( 2.412641546452875208, 19.58572291230954221, -1.500000000000002220 ) ) ;
#4842=CARTESIAN_POINT ( 'NONE',  ( -42.49248349598780550, -24.34968618360933590, 0.1864209137778841952 ) ) ;
#4845=CARTESIAN_POINT ( 'NONE',  ( 4.906390264955167169, 20.09725327650800608, 11.49999999999999645 ) ) ;
#4847=VECTOR ( 'NONE', #16656, 1000.000000000000114 ) ;
#4851=CARTESIAN_POINT ( 'NONE',  ( 5.572475817582897228, 21.94689365879375131, 11.49999999999999645 ) ) ;
#4856=B_SPLINE_CURVE_WITH_KNOTS ( 'NONE', 3,
 ( #50875, #12286, #49888, #80820 ),
 .UNSPECIFIED., .F., .F.,
 ( 4, 4 ),
 ( 0.000000000000000000, 9.999999999997510880E-05 ),
 .UNSPECIFIED. ) ;
#4857=CARTESIAN_POINT ( 'NONE',  ( -60.55620429048339304, -23.47593901973091235, -1.443836447539007972 ) ) ;
#4859=ADVANCED_FACE ( 'NONE', ( #3520 ), #43082, .T. ) ;
#4863=CARTESIAN_POINT ( 'NONE',  ( -100.4426124108961176, -25.12298712672051337, 7.101635559041870494 ) ) ;
#4864=CARTESIAN_POINT ( 'NONE',  ( 5.898633191892585614, -22.09092271590295198, 11.49999999999998934 ) ) ;
#4867=CARTESIAN_POINT ( 'NONE',  ( 0.7969447072908428797, -21.54811710690876225, -1.500000000000002220 ) ) ;
#4868=CARTESIAN_POINT ( 'NONE',  ( -113.5904876474596534, -24.15620529776628800, 10.23563542870659582 ) ) ;
#4869=CARTESIAN_POINT ( 'NONE',  ( -99.16166289166535819, -29.50249453179804249, 5.311361616999957569 ) ) ;
#4870=B_SPLINE_CURVE_WITH_KNOTS ( 'NONE', 3,
 ( #23645, #49011, #11434, #18047, #26666, #79944 ),
 .UNSPECIFIED., .F., .F.,
 ( 4, 2, 4 ),
 ( 0.000000000000000000, 0.001380764517854766700, 0.002761529035709533401 ),
 .UNSPECIFIED. ) ;
#4871=CARTESIAN_POINT ( 'NONE',  ( -5.199590022849982063, -21.90925200621149571, 11.49999999999999645 ) ) ;
#4875=CARTESIAN_POINT ( 'NONE',  ( 19.92286461850947887, -9.344431347164146473, -1.500000000000002220 ) ) ;
#4877=CARTESIAN_POINT ( 'NONE',  ( -111.5158263670924725, -24.34968618360933945, 0.1864209137778883862 ) ) ;
#4878=LINE ( 'NONE', #49065, #28178 ) ;
#4879=ORIENTED_EDGE ( 'NONE', *, *, #44154, .F. ) ;
#4881=CARTESIAN_POINT ( 'NONE',  ( -111.6228709571500559, -23.47593901973091235, -1.443836447538999312 ) ) ;
#4882=ORIENTED_EDGE ( 'NONE', *, *, #55562, .F. ) ;
#4883=CARTESIAN_POINT ( 'NONE',  ( -77.62287095715005592, -24.33832256526968862, 0.1851278514119851781 ) ) ;
#4884=ORIENTED_EDGE ( 'NONE', *, *, #52048, .T. ) ;
#4888=CARTESIAN_POINT ( 'NONE',  ( -65.52287095715011844, -24.82558206586142902, 1.605769216559445711 ) ) ;
#4889=CARTESIAN_POINT ( 'NONE',  ( -42.52287095715005449, -29.50250243563736774, 8.947779886222148704 ) ) ;
#4890=CARTESIAN_POINT ( 'NONE',  ( -57.60487000211600872, -23.73766607897670866, -1.055555164236458454 ) ) ;
#4891=CARTESIAN_POINT ( 'NONE',  ( -15.55180764702766716, 13.24544322234432414, -1.500000000000002220 ) ) ;
#4892=ORIENTED_EDGE ( 'NONE', *, *, #85333, .F. ) ;
#4893=CARTESIAN_POINT ( 'NONE',  ( -128.5228709571500758, -23.47596703998600631, 11.44779298504227683 ) ) ;
#4894=CARTESIAN_POINT ( 'NONE',  ( -115.6228709571500559, -24.99156045073393173, 7.747789690856161648 ) ) ;
#4895=CARTESIAN_POINT ( 'NONE',  ( -105.5848504283774218, -25.00158670708910691, 2.256160236439218369 ) ) ;
#4896=CARTESIAN_POINT ( 'NONE',  ( -71.70841769935766763, -25.03149551985922017, 6.192981911745003565 ) ) ;
#4897=VERTEX_POINT ( 'NONE', #44072 ) ;
#4898=CARTESIAN_POINT ( 'NONE',  ( -123.2228709571500502, -23.47593901973090524, -1.443836447538996426 ) ) ;
#4899=CARTESIAN_POINT ( 'NONE',  ( -86.58953762381672448, -23.48786465467241413, 11.44779295918254469 ) ) ;
#4900=ORIENTED_EDGE ( 'NONE', *, *, #96045, .T. ) ;
#4901=CARTESIAN_POINT ( 'NONE',  ( 10.19739565540945492, -18.13666118385682680, 11.49999999999998934 ) ) ;
#4902=EDGE_CURVE ( 'NONE', #31312, #83417, #33381, .T. ) ;
#4904=CARTESIAN_POINT ( 'NONE',  ( -39.49573010990816613, -25.29496779178032284, 4.491406335818826534 ) ) ;
#4905=ORIENTED_EDGE ( 'NONE', *, *, #17942, .F. ) ;
#4907=CARTESIAN_POINT ( 'NONE',  ( -68.52287095715006160, -23.47596703998600631, 11.44779298504228748 ) ) ;
#4908=CARTESIAN_POINT ( 'NONE',  ( -115.5228709571500190, -24.62226745350438506, 0.9660975649728118508 ) ) ;
#4909=ORIENTED_EDGE ( 'NONE', *, *, #44345, .T. ) ;
#4911=B_SPLINE_CURVE_WITH_KNOTS ( 'NONE', 3,
 ( #67423, #97848, #28851, #44576 ),
 .UNSPECIFIED., .F., .F.,
 ( 4, 4 ),
 ( 0.000000000000000000, 0.0001000000000000167422 ),
 .UNSPECIFIED. ) ;
#4912=CARTESIAN_POINT ( 'NONE',  ( -68.62287095715005592, -29.50247984919015209, -1.443849546365055359 ) ) ;
#4913=CARTESIAN_POINT ( 'NONE',  ( -64.52287095715006160, -23.73934037231756022, 11.05740245334328975 ) ) ;
#4914=FACE_OUTER_BOUND ( 'NONE', #19401, .T. ) ;
#4915=CARTESIAN_POINT ( 'NONE',  ( -43.66335654702338331, -23.48786465467240347, 11.44779295918255180 ) ) ;
#4916=CARTESIAN_POINT ( 'NONE',  ( 11.82310115920509830, 18.66461490495635545, 11.49999999999999645 ) ) ;
#4918=ADVANCED_FACE ( 'NONE', ( #58799 ), #35965, .T. ) ;
#4919=B_SPLINE_CURVE_WITH_KNOTS ( 'NONE', 3,
 ( #27922, #89329, #44151, #27432 ),
 .UNSPECIFIED., .F., .F.,
 ( 4, 4 ),
 ( 0.000000000000000000, 9.999999999998900014E-05 ),
 .UNSPECIFIED. ) ;
#4920=CARTESIAN_POINT ( 'NONE',  ( -108.5923759227193699, -23.96119346886881374, -0.6495511937831862648 ) ) ;
#4921=CARTESIAN_POINT ( 'NONE',  ( 8.141615846073909424, -21.09679883994429161, -1.500000000000002220 ) ) ;
#4922=ADVANCED_FACE ( 'NONE', ( #45081 ), #46078, .T. ) ;
#4923=CARTESIAN_POINT ( 'NONE',  ( -115.5143227195287068, -24.83644354573579349, 8.397322867130096569 ) ) ;
#4924=VERTEX_POINT ( 'NONE', #75502 ) ;
#4926=DIRECTION ( 'NONE',  ( 0.000000000000000000, 2.173523156925980399E-06, -0.9999999999976378895 ) ) ;
#4927=AXIS2_PLACEMENT_3D ( 'NONE', #89375, #95987, #19845 ) ;
#4928=CARTESIAN_POINT ( 'NONE',  ( -57.59299408741310344, -24.15620529776628089, 10.23563542870660470 ) ) ;
#4929=ORIENTED_EDGE ( 'NONE', *, *, #6030, .F. ) ;
#4930=DIRECTION ( 'NONE',  ( -3.773278334453079030E-23, 0.9999999999976377785, 2.173523156925979128E-06 ) ) ;
#4931=CARTESIAN_POINT ( 'NONE',  ( -18.06118310651259407, 13.05043149098080058, -1.500000000000002220 ) ) ;
#4932=DIRECTION ( 'NONE',  ( 3.773278334444167608E-23, -1.000000000000000000, 0.000000000000000000 ) ) ;
#4933=ORIENTED_EDGE ( 'NONE', *, *, #84338, .T. ) ;
#4934=CARTESIAN_POINT ( 'NONE',  ( -42.52287095715005449, -24.65952944569303895, 1.056160979905691910 ) ) ;
#4936=PLANE ( 'NONE',  #64163 ) ;
#4938=B_SPLINE_CURVE_WITH_KNOTS ( 'NONE', 3,
 ( #87057, #79945, #48009, #9933, #9427, #17547 ),
 .UNSPECIFIED., .F., .F.,
 ( 4, 2, 4 ),
 ( 6.391158118975500541E-06, 0.001387004593080798072, 0.002767618028042620644 ),
 .UNSPECIFIED. ) ;
#4940=CARTESIAN_POINT ( 'NONE',  ( -18.23695082634099407, 6.967386181637144738, 11.49999999999998934 ) ) ;
#4941=CARTESIAN_POINT ( 'NONE',  ( -16.73372362409233105, 13.38858591273363174, -1.500000000000002220 ) ) ;
#4944=CARTESIAN_POINT ( 'NONE',  ( -34.52287095715008292, -24.33832256527048088, 0.1851278514138537667 ) ) ;
#4945=CARTESIAN_POINT ( 'NONE',  ( -4.374245501123523283, 22.36648047097513725, -1.500000000000002220 ) ) ;
#4947=EDGE_CURVE ( 'NONE', #72299, #9262, #37461, .T. ) ;
#4951=CARTESIAN_POINT ( 'NONE',  ( 10.26108024787556516, -17.11367029881254709, 11.49999999999999645 ) ) ;
#4954=CARTESIAN_POINT ( 'NONE',  ( -57.22287095715007865, -23.47596703998600276, 11.44779298504227860 ) ) ;
#4956=CARTESIAN_POINT ( 'NONE',  ( -97.52287095715006160, -29.50250243563736774, 8.947779886222138046 ) ) ;
#4957=CARTESIAN_POINT ( 'NONE',  ( -124.5228709571500616, -24.65952944569305316, 1.056160979905705899 ) ) ;
#4958=CARTESIAN_POINT ( 'NONE',  ( 12.82194709444435077, -17.51738216156474337, 11.49999999999998934 ) ) ;
#4960=CARTESIAN_POINT ( 'NONE',  ( -19.08498223313328168, 4.104482590468319536, -1.500000000000002220 ) ) ;
#4962=ORIENTED_EDGE ( 'NONE', *, *, #15618, .T. ) ;
#4965=CARTESIAN_POINT ( 'NONE',  ( -6.584652030910324250, 19.34213596296284265, 11.49999999999999645 ) ) ;
#4966=DIRECTION ( 'NONE',  ( -3.773278334453079618E-23, 0.9999999999976377785, 2.173523156925979975E-06 ) ) ;
#4967=LINE ( 'NONE', #6963, #59438 ) ;
#4968=ADVANCED_FACE ( 'NONE', ( #68409 ), #74847, .T. ) ;
#4973=CARTESIAN_POINT ( 'NONE',  ( -61.62287095715008434, -24.50216790748098816, 0.6166512839513755839 ) ) ;
#4976=CARTESIAN_POINT ( 'NONE',  ( -52.52287095715006870, -24.65952944569303895, 1.056160979905693686 ) ) ;
#4977=EDGE_CURVE ( 'NONE', #31248, #65701, #41849, .T. ) ;
#4979=CARTESIAN_POINT ( 'NONE',  ( 14.37299948674089123, 17.95305339730678185, 11.49999999999999645 ) ) ;
#4980=CARTESIAN_POINT ( 'NONE',  ( 9.298244000614250382, 20.81247324795305431, -1.500000000000002220 ) ) ;
#4984=EDGE_CURVE ( 'NONE', #75656, #54879, #57660, .T. ) ;
#4985=CARTESIAN_POINT ( 'NONE',  ( -74.52287095715003318, -23.73934037231756022, 11.05740245334328975 ) ) ;
#4986=CARTESIAN_POINT ( 'NONE',  ( -110.5487009423575842, -24.92564183028978775, 1.928384488918252204 ) ) ;
#4988=CARTESIAN_POINT ( 'NONE',  ( -9.857428550561325054, -19.57614489166009264, 11.49999999999998934 ) ) ;
#4989=DIRECTION ( 'NONE',  ( -3.773278334453079618E-23, 0.9999999999976377785, 2.173523156925979975E-06 ) ) ;
#4990=DIRECTION ( 'NONE',  ( -3.773278334453079618E-23, 0.9999999999976377785, 2.173523156925979975E-06 ) ) ;
#4991=CARTESIAN_POINT ( 'NONE',  ( -120.6228709571500275, -24.91544648472626378, 1.928969306349428425 ) ) ;
#4994=CARTESIAN_POINT ( 'NONE',  ( 20.14718400222343320, -3.498931157112906476, 11.49999999999998934 ) ) ;
#4995=ORIENTED_EDGE ( 'NONE', *, *, #1253, .F. ) ;
#4997=ORIENTED_EDGE ( 'NONE', *, *, #37112, .T. ) ;
#4998=ORIENTED_EDGE ( 'NONE', *, *, #100417, .F. ) ;
#5000=CARTESIAN_POINT ( 'NONE',  ( 21.75825945658488436, -7.631246777643061030, -1.500000000000002220 ) ) ;
#5001=CARTESIAN_POINT ( 'NONE',  ( -61.49891124310355650, -24.34968618360933945, 0.1864209137778810865 ) ) ;
#5002=CARTESIAN_POINT ( 'NONE',  ( 15.52975653788041122, 12.98207780544785628, -1.500000000000002220 ) ) ;
#5004=CARTESIAN_POINT ( 'NONE',  ( -97.62287095715004170, -23.73907113216991505, -1.053371485793224371 ) ) ;
#5006=CARTESIAN_POINT ( 'NONE',  ( -51.62287095715004881, -24.50321055353805022, 9.387540953477534700 ) ) ;
#5007=CARTESIAN_POINT ( 'NONE',  ( -53.55342350921662842, -23.96169478059712787, 10.65365249895718591 ) ) ;
#5008=CARTESIAN_POINT ( 'NONE',  ( -6.767052838139933080, -20.26514109264706676, 11.49999999999999645 ) ) ;
#5009=ORIENTED_EDGE ( 'NONE', *, *, #80073, .T. ) ;
#5010=CARTESIAN_POINT ( 'NONE',  ( -62.62287095715004881, -29.50247984919015209, -1.443849546365056913 ) ) ;
#5012=VERTEX_POINT ( 'NONE', #88640 ) ;
#5013=CARTESIAN_POINT ( 'NONE',  ( 11.91227609878784399, -18.80521639033699799, -1.500000000000002220 ) ) ;
#5014=CARTESIAN_POINT ( 'NONE',  ( -10.41657757243416604, 17.86655067824183618, -1.500000000000002220 ) ) ;
#5018=CARTESIAN_POINT ( 'NONE',  ( -28.48670877496179799, -24.18537698610731113, 0.1864216068622559508 ) ) ;
#5019=ORIENTED_EDGE ( 'NONE', *, *, #94146, .T. ) ;
#5022=CARTESIAN_POINT ( 'NONE',  ( -18.74228827200876779, -9.293929619069025705, -1.500000000000002220 ) ) ;
#5023=CARTESIAN_POINT ( 'NONE',  ( -21.49438740719132923, 4.340694165963498996, 11.49999999999999645 ) ) ;
#5024=EDGE_CURVE ( 'NONE', #89889, #29980, #56413, .T. ) ;
#5025=CARTESIAN_POINT ( 'NONE',  ( -37.54584601135314159, -24.15620529776627379, 10.23563542870660825 ) ) ;
#5026=CARTESIAN_POINT ( 'NONE',  ( -15.53634343318938704, 16.32316209468629253, -1.500000000000002220 ) ) ;
#5027=CARTESIAN_POINT ( 'NONE',  ( 19.98859412959824411, 6.261702723725245612, 11.49999999999998934 ) ) ;
#5028=ADVANCED_FACE ( 'NONE', ( #90128 ), #58682, .T. ) ;
#5029=CARTESIAN_POINT ( 'NONE',  ( -106.6228709571500559, -23.47596703998600631, 11.44779298504227860 ) ) ;
#5030=CARTESIAN_POINT ( 'NONE',  ( -119.5910506408271914, -23.96169478059714564, 10.65365249895717170 ) ) ;
#5031=DIRECTION ( 'NONE',  ( 0.000000000000000000, -0.9999999999976377785, -2.173523156925979975E-06 ) ) ;
#5033=EDGE_CURVE ( 'NONE', #3088, #46475, #36975, .T. ) ;
#5034=ORIENTED_EDGE ( 'NONE', *, *, #3762, .T. ) ;
#5035=ORIENTED_EDGE ( 'NONE', *, *, #83780, .F. ) ;
#5037=CARTESIAN_POINT ( 'NONE',  ( -11.48222599368078889, -18.13851731312990267, -1.500000000000002220 ) ) ;
#5038=ADVANCED_FACE ( 'NONE', ( #34351 ), #37623, .T. ) ;
#5039=CARTESIAN_POINT ( 'NONE',  ( -42.62287095715004881, -29.50247984919015209, -1.443849546365060466 ) ) ;
#5040=ORIENTED_EDGE ( 'NONE', *, *, #38473, .F. ) ;
#5041=CARTESIAN_POINT ( 'NONE',  ( 15.50021099394596646, 14.30638080151107694, -1.500000000000002220 ) ) ;
#5042=CARTESIAN_POINT ( 'NONE',  ( -70.30743594849178635, -25.23380821724332534, 3.513009940249934182 ) ) ;
#5044=CARTESIAN_POINT ( 'NONE',  ( -50.60039650190779525, -24.15602025860895452, 10.28564288303536856 ) ) ;
#5046=CARTESIAN_POINT ( 'NONE',  ( -99.17216252687966005, -25.23367668196706504, 3.679805935859953081 ) ) ;
#5047=CARTESIAN_POINT ( 'NONE',  ( -22.12685673520133989, -0.1325007643398395663, -1.500000000000002220 ) ) ;
#5048=DIRECTION ( 'NONE',  ( 0.000000000000000000, 2.173523156925980399E-06, -0.9999999999976378895 ) ) ;
#5050=CARTESIAN_POINT ( 'NONE',  ( -56.52287095715009002, -23.72773821059536203, 11.05748984161097503 ) ) ;
#5051=CARTESIAN_POINT ( 'NONE',  ( -41.86646858058957577, -25.31624481711344643, 4.347423942039069900 ) ) ;
#5052=B_SPLINE_CURVE_WITH_KNOTS ( 'NONE', 3,
 ( #63867, #71462, #1950, #1449 ),
 .UNSPECIFIED., .F., .F.,
 ( 4, 4 ),
 ( 0.2789617571284340736, 0.2799625041691996552 ),
 .UNSPECIFIED. ) ;
#5053=CARTESIAN_POINT ( 'NONE',  ( -100.5908750829490117, -24.40034930558990567, 0.3402023900116026844 ) ) ;
#5054=B_SPLINE_CURVE_WITH_KNOTS ( 'NONE', 3,
 ( #60242, #68839, #59739, #5436, #84055, #14034, #5932, #36885 ),
 .UNSPECIFIED., .F., .F.,
 ( 4, 2, 2, 4 ),
 ( 6.384118678621298445E-06, 0.002007151183507261457, 0.003007534715921583376, 0.004007918248335905730 ),
 .UNSPECIFIED. ) ;
#5055=CARTESIAN_POINT ( 'NONE',  ( 12.02608574658498597, -17.65016651952024063, 11.49999999999998934 ) ) ;
#5056=CARTESIAN_POINT ( 'NONE',  ( -70.25323322593359876, -25.04378563015144010, 7.559868539947981247 ) ) ;
#5057=DIRECTION ( 'NONE',  ( -3.773278334453079618E-23, 0.9999999999976377785, 2.173523156925979975E-06 ) ) ;
#5059=FACE_OUTER_BOUND ( 'NONE', #27478, .T. ) ;
#5061=CARTESIAN_POINT ( 'NONE',  ( 21.95517018727266390, 5.574673621280945568, -1.500000000000002220 ) ) ;
#5062=EDGE_LOOP ( 'NONE', ( #28717, #23049, #49464, #40104 ) ) ;
#5063=CARTESIAN_POINT ( 'NONE',  ( -109.9228709571500673, -23.47593901973090524, -1.443836447538996426 ) ) ;
#5064=CARTESIAN_POINT ( 'NONE',  ( -69.62287095715005592, -23.47593901973091235, -1.443836447539006196 ) ) ;
#5065=CARTESIAN_POINT ( 'NONE',  ( -17.00503767097633556, -9.977476526402845991, 11.49999999999999645 ) ) ;
#5067=CARTESIAN_POINT ( 'NONE',  ( -59.62287095715007723, -23.47596703998600276, 11.44779298504227683 ) ) ;
#5068=ORIENTED_EDGE ( 'NONE', *, *, #14290, .T. ) ;
#5071=PLANE ( 'NONE',  #83853 ) ;
#5072=CARTESIAN_POINT ( 'NONE',  ( 11.61936018155104833, -18.21891831228114356, -1.500000000000002220 ) ) ;
#5073=CARTESIAN_POINT ( 'NONE',  ( -27.38110673051268762, -24.78324009960318364, 7.572115309721827003 ) ) ;
#5074=CARTESIAN_POINT ( 'NONE',  ( 8.665315094346039970, 17.34094453737590769, -1.500000000000002220 ) ) ;
#5076=CARTESIAN_POINT ( 'NONE',  ( -80.51244414166535535, -25.04307398257883577, 7.563174194274490780 ) ) ;
#5077=CARTESIAN_POINT ( 'NONE',  ( 19.60560811685724403, 2.727087469661350738, 11.49999999999998934 ) ) ;
#5081=CARTESIAN_POINT ( 'NONE',  ( -20.27173212042777806, -0.06527795377243154895, 11.49999999999999645 ) ) ;
#5082=CARTESIAN_POINT ( 'NONE',  ( -119.5228709571500758, -23.48786465467241769, 11.44779295918253759 ) ) ;
#5084=ADVANCED_FACE ( 'NONE', ( #97736 ), #51573, .T. ) ;
#5085=VERTEX_POINT ( 'NONE', #2914 ) ;
#5087=CARTESIAN_POINT ( 'NONE',  ( -88.52287095715006160, -23.48786465467241769, 11.44779295918254292 ) ) ;
#5088=CARTESIAN_POINT ( 'NONE',  ( -44.62287095715007013, -24.34917612406837861, 0.1852690917426601802 ) ) ;
#5092=CARTESIAN_POINT ( 'NONE',  ( 16.02535498940104830, 12.03463022438520191, -1.500000000000002220 ) ) ;
#5093=EDGE_CURVE ( 'NONE', #94029, #18132, #13955, .T. ) ;
#5099=DIRECTION ( 'NONE',  ( -3.773278334453079618E-23, 0.9999999999976377785, 2.173523156925978705E-06 ) ) ;
#5100=CARTESIAN_POINT ( 'NONE',  ( -67.52287095715006160, -23.48786465467241769, 11.44779295918254647 ) ) ;
#5101=EDGE_CURVE ( 'NONE', #5695, #5245, #18819, .T. ) ;
#5102=DIRECTION ( 'NONE',  ( -1.000000000000000000, -3.773278334444167608E-23, -8.201307833595939069E-29 ) ) ;
#5103=PLANE ( 'NONE',  #62467 ) ;
#5105=CARTESIAN_POINT ( 'NONE',  ( -14.11974515630795501, -17.41659395067913962, 11.49999999999999645 ) ) ;
#5106=CARTESIAN_POINT ( 'NONE',  ( -49.26475614252912294, -25.23256535379771037, 6.480020017899467355 ) ) ;
#5107=VERTEX_POINT ( 'NONE', #74887 ) ;
#5108=CARTESIAN_POINT ( 'NONE',  ( 18.28078834835902455, 8.925752885971231620, 11.49999999999998934 ) ) ;
#5109=ORIENTED_EDGE ( 'NONE', *, *, #81874, .T. ) ;
#5110=EDGE_CURVE ( 'NONE', #39996, #100298, #91612, .T. ) ;
#5111=CARTESIAN_POINT ( 'NONE',  ( -6.529369910325518944, -22.02198592821369516, 11.49999999999998934 ) ) ;
#5113=ORIENTED_EDGE ( 'NONE', *, *, #96784, .T. ) ;
#5116=ADVANCED_FACE ( 'NONE', ( #5390 ), #68791, .F. ) ;
#5117=CARTESIAN_POINT ( 'NONE',  ( -38.62287095715005592, -24.66019654487199020, 8.947790411086137041 ) ) ;
#5118=CARTESIAN_POINT ( 'NONE',  ( -21.08002519818654363, -2.465602145356518893, 11.49999999999999645 ) ) ;
#5120=B_SPLINE_CURVE_WITH_KNOTS ( 'NONE', 3,
 ( #24965, #33088, #49330, #47815, #39188, #1140 ),
 .UNSPECIFIED., .F., .F.,
 ( 4, 2, 4 ),
 ( 1.570755371634111329E-05, 0.001396183895866087103, 0.002776660238015833410 ),
 .UNSPECIFIED. ) ;
#5122=CARTESIAN_POINT ( 'NONE',  ( -14.74362065938029076, 16.57599527146691898, -1.500000000000002220 ) ) ;
#5124=CARTESIAN_POINT ( 'NONE',  ( 10.47388184937329214, 17.72644800832989986, 11.49999999999998934 ) ) ;
#5128=CARTESIAN_POINT ( 'NONE',  ( -82.62287095715005592, -29.50248528299804818, 1.056150453629038477 ) ) ;
#5132=DIRECTION ( 'NONE',  ( -3.773278334444167608E-23, 1.000000000000000000, 0.000000000000000000 ) ) ;
#5133=CARTESIAN_POINT ( 'NONE',  ( -28.57183748306234250, -23.32756358287736376, 11.44779300624184160 ) ) ;
#5135=CARTESIAN_POINT ( 'NONE',  ( -12.26507114386991226, -16.75673120704366426, -1.500000000000002220 ) ) ;
#5136=CARTESIAN_POINT ( 'NONE',  ( 15.29254711327534899, -15.47666941828629739, 11.49999999999999645 ) ) ;
#5137=ORIENTED_EDGE ( 'NONE', *, *, #1504, .F. ) ;
#5138=CARTESIAN_POINT ( 'NONE',  ( -100.6399447160575420, -25.18730714472780718, 3.310768607064317415 ) ) ;
#5140=CARTESIAN_POINT ( 'NONE',  ( -37.55620429048340014, -24.66019654487198665, 8.947790411086135265 ) ) ;
#5141=FACE_OUTER_BOUND ( 'NONE', #45197, .T. ) ;
#5142=CARTESIAN_POINT ( 'NONE',  ( -22.40390758644239710, -1.035154934579901820, -1.500000000000002220 ) ) ;
#5145=CARTESIAN_POINT ( 'NONE',  ( -65.59841495659875932, -24.15503026093916006, -0.2815557561904380446 ) ) ;
#5146=ORIENTED_EDGE ( 'NONE', *, *, #41140, .F. ) ;
#5147=CARTESIAN_POINT ( 'NONE',  ( -71.27031559404676386, -25.31598477088890320, 4.985721588723864173 ) ) ;
#5149=CARTESIAN_POINT ( 'NONE',  ( -95.52287095715006160, -24.99156044556203327, 7.747789690856173195 ) ) ;
#5152=EDGE_LOOP ( 'NONE', ( #71179, #74921, #81521, #63344 ) ) ;
#5153=EDGE_CURVE ( 'NONE', #78417, #60824, #69689, .T. ) ;
#5154=CARTESIAN_POINT ( 'NONE',  ( -99.52318946800619415, -25.30202668977020863, 5.579290425899357864 ) ) ;
#5156=CARTESIAN_POINT ( 'NONE',  ( 4.979423480801214552, 20.69870207611912605, -1.500000000000002220 ) ) ;
#5157=ORIENTED_EDGE ( 'NONE', *, *, #55762, .T. ) ;
#5159=CARTESIAN_POINT ( 'NONE',  ( 16.32745387341675780, -14.53119815553504068, -1.500000000000002220 ) ) ;
#5160=DIRECTION ( 'NONE',  ( 0.000000000000000000, -2.173523156925979552E-06, 0.9999999999976378895 ) ) ;
#5161=CARTESIAN_POINT ( 'NONE',  ( 13.52301212282245935, 18.22803923376396540, -1.500000000000002220 ) ) ;
#5162=FACE_OUTER_BOUND ( 'NONE', #92728, .T. ) ;
#5164=CARTESIAN_POINT ( 'NONE',  ( -13.81295463269534096, 17.03802364079049525, -1.500000000000002220 ) ) ;
#5165=CARTESIAN_POINT ( 'NONE',  ( -87.58567460725342357, -24.51314013834317151, 0.6176544820404251679 ) ) ;
#5168=CARTESIAN_POINT ( 'NONE',  ( -121.6228709571500417, -23.47593901973091235, -1.443836447538997536 ) ) ;
#5170=CARTESIAN_POINT ( 'NONE',  ( -84.51766182033699693, -23.73791477778912551, 11.05961554403170766 ) ) ;
#5171=CARTESIAN_POINT ( 'NONE',  ( -41.62287095715007013, -24.51283580621364422, 0.6167428607019734832 ) ) ;
#5172=CARTESIAN_POINT ( 'NONE',  ( -20.43740209601095614, -23.59208382403500437, 0.3010598746230517819 ) ) ;
#5173=CARTESIAN_POINT ( 'NONE',  ( -18.64022381217131397, 10.26305532446727753, 11.49999999999998934 ) ) ;
#5174=CARTESIAN_POINT ( 'NONE',  ( -98.50756231633036464, -24.66019654487200086, 8.947790411086115725 ) ) ;
#5175=CARTESIAN_POINT ( 'NONE',  ( -26.55847933594999333, -24.75186106919953488, 2.904080373301505702 ) ) ;
#5176=CARTESIAN_POINT ( 'NONE',  ( -75.62287095715005592, -29.50250786944525672, 11.44777988621623521 ) ) ;
#5177=CARTESIAN_POINT ( 'NONE',  ( -33.62373644273809958, -24.65952944569304606, 1.056160979905695907 ) ) ;
#5180=CARTESIAN_POINT ( 'NONE',  ( -117.5222355272872221, -23.48786465467241769, 11.44779295918253581 ) ) ;
#5182=CARTESIAN_POINT ( 'NONE',  ( 19.50827032651345405, -1.201405007418623994, 11.49999999999999645 ) ) ;
#5184=CARTESIAN_POINT ( 'NONE',  ( -68.58953762381672448, -24.64898659630367916, 1.056161002820382722 ) ) ;
#5185=ORIENTED_EDGE ( 'NONE', *, *, #91117, .T. ) ;
#5187=CARTESIAN_POINT ( 'NONE',  ( -99.30277203926080176, -25.25095956454628521, 6.024134243369381636 ) ) ;
#5188=CARTESIAN_POINT ( 'NONE',  ( -26.12253190299266237, -24.72833061199699500, 7.423757303530043927 ) ) ;
#5189=CARTESIAN_POINT ( 'NONE',  ( -40.62287095715006302, -24.62285846362214414, 9.038163152653526211 ) ) ;
#5190=CARTESIAN_POINT ( 'NONE',  ( -19.47062899137607772, 3.135797168518691169, 11.49999999999998934 ) ) ;
#5191=ORIENTED_EDGE ( 'NONE', *, *, #72872, .F. ) ;
#5195=B_SPLINE_CURVE_WITH_KNOTS ( 'NONE', 3,
 ( #48245, #24390, #64494, #93393 ),
 .UNSPECIFIED., .F., .F.,
 ( 4, 4 ),
 ( 0.000000000000000000, 1.000000000000000000 ),
 .UNSPECIFIED. ) ;
#5198=ORIENTED_EDGE ( 'NONE', *, *, #65771, .T. ) ;
#5201=CARTESIAN_POINT ( 'NONE',  ( -47.64621855144071105, -23.96119346886880663, -0.6495511937831951466 ) ) ;
#5202=CARTESIAN_POINT ( 'NONE',  ( -118.5191058840536869, -24.15543982623907482, -0.2315651400026558782 ) ) ;
#5203=CARTESIAN_POINT ( 'NONE',  ( -45.62287095715004881, -24.99156045073392463, 7.747789690856161648 ) ) ;
#5204=EDGE_CURVE ( 'NONE', #642, #55321, #28520, .T. ) ;
#5205=CARTESIAN_POINT ( 'NONE',  ( -99.62287095715008434, -24.51387760970723306, 9.387446482453400520 ) ) ;
#5206=CARTESIAN_POINT ( 'NONE',  ( -107.5144731571734127, -24.34968618360934656, 0.1864209137778970737 ) ) ;
#5207=CARTESIAN_POINT ( 'NONE',  ( -8.813339738934139689, -17.91118242276673911, -1.500000000000002220 ) ) ;
#5208=EDGE_CURVE ( 'NONE', #896, #19866, #5519, .T. ) ;
#5209=CARTESIAN_POINT ( 'NONE',  ( -71.52287095715006160, -23.47593901973090169, -1.443836447538996870 ) ) ;
#5211=DIRECTION ( 'NONE',  ( -3.773278334453079030E-23, 0.9999999999976377785, 2.173523156925979128E-06 ) ) ;
#5213=CARTESIAN_POINT ( 'NONE',  ( -128.6228709571500417, -23.48786465467242479, 11.44779295918253403 ) ) ;
#5215=EDGE_CURVE ( 'NONE', #46438, #67086, #55143, .T. ) ;
#5216=VECTOR ( 'NONE', #32004, 1000.000000000000114 ) ;
#5218=CARTESIAN_POINT ( 'NONE',  ( -80.64005565590667857, -24.15602025860896163, 10.28564288303536145 ) ) ;
#5219=CARTESIAN_POINT ( 'NONE',  ( -49.62287095715007013, -24.35013146730203459, 9.818937971375108376 ) ) ;
#5220=CARTESIAN_POINT ( 'NONE',  ( -81.49977361814643473, -24.65952944569304961, 1.056160979905703901 ) ) ;
#5221=EDGE_CURVE ( 'NONE', #153, #32461, #17491, .T. ) ;
#5223=CARTESIAN_POINT ( 'NONE',  ( -51.33061876479827390, -25.26280066856253015, 4.756068594975189079 ) ) ;
#5224=VERTEX_POINT ( 'NONE', #93108 ) ;
#5225=CARTESIAN_POINT ( 'NONE',  ( -37.62287095715006302, -24.50321055353804311, 9.387540953477531147 ) ) ;
#5228=CARTESIAN_POINT ( 'NONE',  ( 10.87751022112437482, 17.06716278085755079, 11.49999999999998934 ) ) ;
#5229=CARTESIAN_POINT ( 'NONE',  ( -43.58953762381671027, -23.48783264082477729, -1.443836473390071928 ) ) ;
#5231=CARTESIAN_POINT ( 'NONE',  ( -109.6228709571500701, -23.72747288104441665, -1.053458166803660667 ) ) ;
#5232=B_SPLINE_CURVE_WITH_KNOTS ( 'NONE', 3,
 ( #33288, #2866, #64275, #25681, #87589, #79966, #10452, #70360, #41415, #72371 ),
 .UNSPECIFIED., .F., .F.,
 ( 4, 2, 2, 2, 4 ),
 ( 8.673617379884034509E-19, 0.0001781668809738670191, 0.0003563337619477331708, 0.0007126675238954626552, 0.001425335047790923793 ),
 .UNSPECIFIED. ) ;
#5234=CARTESIAN_POINT ( 'NONE',  ( -80.16754667335695217, -25.30573843112062349, 4.512742708063584907 ) ) ;
#5236=CARTESIAN_POINT ( 'NONE',  ( -11.36185547594953249, 16.55520930037988592, -1.500000000000002220 ) ) ;
#5237=CARTESIAN_POINT ( 'NONE',  ( 20.56459456670464547, 4.482388377596099538, 11.49999999999999645 ) ) ;
#5238=CARTESIAN_POINT ( 'NONE',  ( -28.04258906917542404, -24.84821647549576795, 7.555446715630902865 ) ) ;
#5239=CARTESIAN_POINT ( 'NONE',  ( -70.49291431472521197, -24.73531770709095312, 8.716586749053510275 ) ) ;
#5240=CARTESIAN_POINT ( 'NONE',  ( -19.65368394218270254, -10.04821906498216499, -1.500000000000002220 ) ) ;
#5244=CARTESIAN_POINT ( 'NONE',  ( -64.62287095715007013, -23.47596703998600631, 11.44779298504227683 ) ) ;
#5245=VERTEX_POINT ( 'NONE', #32210 ) ;
#5246=CARTESIAN_POINT ( 'NONE',  ( -100.0333332052708926, -25.13022549009045292, 2.886596846642130565 ) ) ;
#5247=CARTESIAN_POINT ( 'NONE',  ( -31.58668462884854478, -24.34968618360933590, 0.1864209137778850556 ) ) ;
#5250=PLANE ( 'NONE',  #25931 ) ;
#5251=DIRECTION ( 'NONE',  ( -1.000000000000000000, -3.773278334444167608E-23, -8.201307837791369499E-29 ) ) ;
#5252=CARTESIAN_POINT ( 'NONE',  ( -76.63010910783911811, -24.34968618360934300, 0.1864209137778859160 ) ) ;
#5253=CARTESIAN_POINT ( 'NONE',  ( -1.637206367458305500, 20.51943892441452633, -1.500000000000002220 ) ) ;
#5254=CARTESIAN_POINT ( 'NONE',  ( 13.05104812959431548, -17.15854754814989391, 11.49999999999999645 ) ) ;
#5255=EDGE_LOOP ( 'NONE', ( #33093, #72521, #79588, #90524 ) ) ;
#5256=CARTESIAN_POINT ( 'NONE',  ( -91.60160660209938044, -23.48783264082477018, -1.443836473390090802 ) ) ;
#5257=CARTESIAN_POINT ( 'NONE',  ( -56.62287095715004881, -24.66019654487199020, 8.947790411086131712 ) ) ;
#5258=CARTESIAN_POINT ( 'NONE',  ( -129.6228709571500417, -24.65952944569305316, 1.056160979905706121 ) ) ;
#5259=CARTESIAN_POINT ( 'NONE',  ( 3.003370282714790562, 22.13870467353671856, -1.500000000000002220 ) ) ;
#5260=CARTESIAN_POINT ( 'NONE',  ( -79.68206046389329344, -25.27875020210991863, 6.776761220936831087 ) ) ;
#5261=CARTESIAN_POINT ( 'NONE',  ( -61.55620429048339304, -24.64898659630528854, 1.056161002820821260 ) ) ;
#5262=ORIENTED_EDGE ( 'NONE', *, *, #82532, .F. ) ;
#5264=CARTESIAN_POINT ( 'NONE',  ( -59.62287095715004881, -29.50247984919015209, -1.443849546365056913 ) ) ;
#5265=AXIS2_PLACEMENT_3D ( 'NONE', #19551, #42910, #1844 ) ;
#5266=CARTESIAN_POINT ( 'NONE',  ( -17.14161228048114438, 11.91956482804130601, 11.49999999999998934 ) ) ;
#5268=ADVANCED_FACE ( 'NONE', ( #47450 ), #63697, .F. ) ;
#5271=VERTEX_POINT ( 'NONE', #77376 ) ;
#5272=CARTESIAN_POINT ( 'NONE',  ( -100.6244603630846512, -24.92592662359561118, 8.075495903017998245 ) ) ;
#5273=CARTESIAN_POINT ( 'NONE',  ( -9.089321149825819290, -19.05894737874082168, -1.500000000000002220 ) ) ;
#5274=EDGE_CURVE ( 'NONE', #71653, #4511, #89101, .T. ) ;
#5276=CARTESIAN_POINT ( 'NONE',  ( -77.62287095715005592, -24.64898659630367916, 1.056161002820826145 ) ) ;
#5278=LINE ( 'NONE', #35742, #49745 ) ;
#5279=CARTESIAN_POINT ( 'NONE',  ( -76.58805659134553423, -24.35071581493543036, 9.817618358456028815 ) ) ;
#5280=CARTESIAN_POINT ( 'NONE',  ( -89.52287095715006160, -29.50247984919015209, -1.443849546365051806 ) ) ;
#5281=CARTESIAN_POINT ( 'NONE',  ( -19.00758693998263738, -10.61793046214600089, -1.500000000000002220 ) ) ;
#5283=CARTESIAN_POINT ( 'NONE',  ( -0.5504121640580519337, 22.28327991085032878, 11.49999999999999645 ) ) ;
#5284=VERTEX_POINT ( 'NONE', #56070 ) ;
#5285=CARTESIAN_POINT ( 'NONE',  ( -57.52287095715004739, -23.96177878511308634, 10.65340807706330217 ) ) ;
#5287=CARTESIAN_POINT ( 'NONE',  ( -31.58953762381672803, -24.64898659630367206, 1.056161002820377393 ) ) ;
#5288=EDGE_LOOP ( 'NONE', ( #35843, #64085, #56963, #83818 ) ) ;
#5291=ORIENTED_EDGE ( 'NONE', *, *, #44620, .F. ) ;
#5294=DIRECTION ( 'NONE',  ( -0.000000000000000000, 2.173523156925979552E-06, -0.9999999999976378895 ) ) ;
#5296=B_SPLINE_CURVE_WITH_KNOTS ( 'NONE', 3,
 ( #54215, #27986, #61823, #36097, #97976, #59440 ),
 .UNSPECIFIED., .F., .F.,
 ( 4, 2, 4 ),
 ( 6.391158118972359742E-06, 0.001387004593080792651, 0.002767618028042612838 ),
 .UNSPECIFIED. ) ;
#5297=DIRECTION ( 'NONE',  ( -3.773278334453079030E-23, 0.9999999999976377785, 2.173523156925979128E-06 ) ) ;
#5298=CARTESIAN_POINT ( 'NONE',  ( -19.23900614489824079, 2.250179475969715348, -1.500000000000002220 ) ) ;
#5300=EDGE_LOOP ( 'NONE', ( #28980, #59107, #16887, #25208 ) ) ;
#5301=CARTESIAN_POINT ( 'NONE',  ( 12.39309347844599252, 14.90900669795185252, 11.49999999999999645 ) ) ;
#5302=CARTESIAN_POINT ( 'NONE',  ( -69.52287095715009002, -23.72747288104470442, -1.053458166803227014 ) ) ;
#5304=ORIENTED_EDGE ( 'NONE', *, *, #86725, .F. ) ;
#5306=CARTESIAN_POINT ( 'NONE',  ( -116.6228709571500559, -29.50248528299804818, 1.056150453629045360 ) ) ;
#5308=CARTESIAN_POINT ( 'NONE',  ( -87.62287095715004170, -24.64965695001468404, 8.947790433994180503 ) ) ;
#5309=CARTESIAN_POINT ( 'NONE',  ( 11.71876819965036809, 15.69520123712499249, 11.49999999999998934 ) ) ;
#5310=B_SPLINE_SURFACE_WITH_KNOTS ( 'NONE', 3, 3, ( 
 ( #92517, #24507, #71197, #32122 ),
 ( #46352, #7785, #100107, #674 ),
 ( #16391, #15391, #62586, #46856 ),
 ( #53487, #7280, #63094, #53979 ),
 ( #84413, #85405, #32625, #69696 ),
 ( #93512, #62092, #63601, #47358 ),
 ( #84906, #78287, #31621, #94523 ) ),
 .UNSPECIFIED., .F., .F., .F.,
 ( 4, 3, 4 ),
 ( 4, 4 ),
 ( 0.0004766839783823226305, 0.1029713700210898170, 0.2054660560637973088 ),
 ( 0.3595854696482522206, 0.3607641062792684150 ),
 .UNSPECIFIED. ) ;
#5311=CARTESIAN_POINT ( 'NONE',  ( -46.53515119466756289, -24.51314013834315020, 0.6176544820404062941 ) ) ;
#5313=CARTESIAN_POINT ( 'NONE',  ( -19.35566633068252074, -9.524217769563914970, -1.500000000000002220 ) ) ;
#5315=CARTESIAN_POINT ( 'NONE',  ( -70.42265764498320380, -25.12219144110324720, 7.098707687581576664 ) ) ;
#5316=CARTESIAN_POINT ( 'NONE',  ( -120.6228709571500417, -29.50249982740957577, 7.747779886224967605 ) ) ;
#5317=CARTESIAN_POINT ( 'NONE',  ( -100.3381132846150052, -25.18439336221437941, 3.296131460420185011 ) ) ;
#5318=CARTESIAN_POINT ( 'NONE',  ( -15.63304604236160067, -16.83380969201049382, -1.500000000000002220 ) ) ;
#5322=CARTESIAN_POINT ( 'NONE',  ( -49.49801449864284564, -25.25249061358302782, 3.767456410489268936 ) ) ;
#5323=CARTESIAN_POINT ( 'NONE',  ( -12.46103870137906711, 15.87156016069071462, 11.49999999999999645 ) ) ;
#5324=CARTESIAN_POINT ( 'NONE',  ( -108.9585383990916796, -25.28814330945115785, 4.038060318331745613 ) ) ;
#5325=CARTESIAN_POINT ( 'NONE',  ( -32.65887063574198379, -23.73791477778911485, 11.05961554403171299 ) ) ;
#5327=ADVANCED_FACE ( 'NONE', ( #46447 ), #70786, .F. ) ;
#5330=LINE ( 'NONE', #37284, #18614 ) ;
#5331=CARTESIAN_POINT ( 'NONE',  ( -7.150643268323968904, -18.52920452239153448, -1.500000000000002220 ) ) ;
#5334=CARTESIAN_POINT ( 'NONE',  ( -113.5554278171332925, -23.96119346886881019, -0.6495511937832028071 ) ) ;
#5335=CARTESIAN_POINT ( 'NONE',  ( 18.95923836289803788, 5.684714004613049987, -1.500000000000002220 ) ) ;
#5336=CARTESIAN_POINT ( 'NONE',  ( -126.6239566813304975, -24.35071581493544457, 9.817618358456011052 ) ) ;
#5338=B_SPLINE_CURVE_WITH_KNOTS ( 'NONE', 3,
 ( #12142, #50228, #33491, #41118, #66477, #3058 ),
 .UNSPECIFIED., .F., .F.,
 ( 4, 2, 4 ),
 ( 6.384118678608765745E-06, 0.001386860460828372383, 0.002767336802978136254 ),
 .UNSPECIFIED. ) ;
#5342=CARTESIAN_POINT ( 'NONE',  ( -51.29687923781917647, -29.50249166729307149, 3.993452963156916002 ) ) ;
#5344=CARTESIAN_POINT ( 'NONE',  ( 18.27903665858761073, 9.701928907310005457, 11.49999999999999645 ) ) ;
#5345=DIRECTION ( 'NONE',  ( -3.773278334453079618E-23, 0.9999999999976377785, 2.173523156925979975E-06 ) ) ;
#5347=CARTESIAN_POINT ( 'NONE',  ( -127.5228709571500616, -29.50248528299804818, 1.056150453629047137 ) ) ;
#5348=FACE_OUTER_BOUND ( 'NONE', #19014, .T. ) ;
#5349=CARTESIAN_POINT ( 'NONE',  ( -0.4833002549469566644, -22.66139224067150337, 11.49999999999999645 ) ) ;
#5351=CARTESIAN_POINT ( 'NONE',  ( -67.52287095715004739, -23.94994826722565406, -0.6494450866342734718 ) ) ;
#5352=CARTESIAN_POINT ( 'NONE',  ( -33.52287095715006160, -24.66019654487198665, 8.947790411086131712 ) ) ;
#5354=CARTESIAN_POINT ( 'NONE',  ( -100.5228709571500616, -29.50250243563736774, 8.947779886222138046 ) ) ;
#5356=VERTEX_POINT ( 'NONE', #26107 ) ;
#5359=CARTESIAN_POINT ( 'NONE',  ( -98.52287095715006160, -29.50248528299804818, 1.056150453629042030 ) ) ;
#5360=CARTESIAN_POINT ( 'NONE',  ( -22.23020047961643186, 5.420056861400933457, 11.49999999999998934 ) ) ;
#5362=CARTESIAN_POINT ( 'NONE',  ( 16.61904782137575154, -13.72857183568914685, -1.500000000000002220 ) ) ;
#5363=DIRECTION ( 'NONE',  ( -3.773278334444166432E-23, 1.000000000000000000, 0.000000000000000000 ) ) ;
#5364=CARTESIAN_POINT ( 'NONE',  ( -65.52287095715010423, -24.63287334234179937, 0.9662140553045344138 ) ) ;
#5366=CARTESIAN_POINT ( 'NONE',  ( -8.633696204196466439, -20.85254729778420923, 11.49999999999999645 ) ) ;
#5367=ORIENTED_EDGE ( 'NONE', *, *, #47058, .F. ) ;
#5368=DIRECTION ( 'NONE',  ( 1.000000000000000000, 3.773278334444167608E-23, 8.201307833595939069E-29 ) ) ;
#5369=CARTESIAN_POINT ( 'NONE',  ( -6.321128248299066499, 21.05883132939252533, 11.49999999999998934 ) ) ;
#5371=PLANE ( 'NONE',  #78343 ) ;
#5373=ORIENTED_EDGE ( 'NONE', *, *, #91916, .T. ) ;
#5374=CARTESIAN_POINT ( 'NONE',  ( -48.52204675041186732, -23.48786465467241058, 11.44779295918254824 ) ) ;
#5375=CARTESIAN_POINT ( 'NONE',  ( -90.55814612579646905, -23.85049219812686871, 10.88485053497527844 ) ) ;
#5377=LINE ( 'NONE', #90609, #79315 ) ;
#5379=VECTOR ( 'NONE', #38987, 1000.000000000000114 ) ;
#5384=CARTESIAN_POINT ( 'NONE',  ( -17.38880980700008294, 10.71821138944157603, -1.500000000000002220 ) ) ;
#5385=VERTEX_POINT ( 'NONE', #28109 ) ;
#5387=CARTESIAN_POINT ( 'NONE',  ( -115.6228709571500417, -24.82576562982393042, 8.398263435472966165 ) ) ;
#5388=EDGE_CURVE ( 'NONE', #92355, #63898, #32115, .T. ) ;
#5389=CARTESIAN_POINT ( 'NONE',  ( -105.5477505147810717, -24.83618233451451118, 1.606449574219534826 ) ) ;
#5390=FACE_OUTER_BOUND ( 'NONE', #19136, .T. ) ;
#5391=EDGE_LOOP ( 'NONE', ( #19516, #48825, #56348, #37953 ) ) ;
#5392=FACE_OUTER_BOUND ( 'NONE', #6046, .T. ) ;
#5393=CARTESIAN_POINT ( 'NONE',  ( -27.70544111104076990, -25.26248076824083100, 8.251825376808540113 ) ) ;
#5394=CARTESIAN_POINT ( 'NONE',  ( 5.792680761630559338, -19.98616098212858105, -1.500000000000002220 ) ) ;
#5396=EDGE_CURVE ( 'NONE', #24728, #153, #91412, .T. ) ;
#5397=B_SPLINE_CURVE_WITH_KNOTS ( 'NONE', 3,
 ( #27760, #51600, #20138, #82046 ),
 .UNSPECIFIED., .F., .F.,
 ( 4, 4 ),
 ( 1.387778780781445521E-17, 0.0001000000000000028779 ),
 .UNSPECIFIED. ) ;
#5400=B_SPLINE_SURFACE_WITH_KNOTS ( 'NONE', 3, 1, ( 
 ( #13286, #21390 ),
 ( #12290, #43266 ),
 ( #58992, #5187 ),
 ( #13784, #36143 ),
 ( #44261, #75683 ),
 ( #36635, #34653 ),
 ( #4199, #11799 ),
 ( #58004, #88936 ),
 ( #42773, #19411 ),
 ( #73706, #37135 ),
 ( #16295, #85304 ),
 ( #84804, #68097 ),
 ( #15791, #76183 ),
 ( #70088, #45257 ),
 ( #7178, #571 ),
 ( #38127, #47258 ),
 ( #61488, #37633 ),
 ( #99019, #83806 ),
 ( #30520, #91915 ) ),
 .UNSPECIFIED., .F., .F., .F.,
 ( 4, 1, 1, 1, 1, 1, 1, 1, 1, 1, 1, 1, 1, 1, 1, 1, 4 ),
 ( 2, 2 ),
 ( 0.000000000000000000, 0.06690918560565620177, 0.1334854404229647851, 0.2010351165700799414, 0.2712343400187647857, 0.3428799841615815525, 0.4138361296100178666, 0.4859766219744184323, 0.5602295572555456848, 0.5998841807523912495, 0.6440548396425977984, 0.6918919315842514406, 0.7446875244737690691, 0.8014917751698753534, 0.8628576982200926171, 0.9293283793947423321, 1.000000000000000000 ),
 ( 0.000000000000000000, 1.000000000000000000 ),
 .UNSPECIFIED. ) ;
#5401=LINE ( 'NONE', #6400, #85960 ) ;
#5402=CARTESIAN_POINT ( 'NONE',  ( -129.5895789150353323, -24.66019654487200086, 8.947790411086113949 ) ) ;
#5403=ORIENTED_EDGE ( 'NONE', *, *, #40864, .F. ) ;
#5404=ORIENTED_EDGE ( 'NONE', *, *, #71191, .F. ) ;
#5405=CARTESIAN_POINT ( 'NONE',  ( -29.62287095715005592, -24.42603767492987998, 0.6165372256073464730 ) ) ;
#5408=B_SPLINE_CURVE_WITH_KNOTS ( 'NONE', 3,
 ( #47354, #10289, #2193, #93509 ),
 .UNSPECIFIED., .F., .F.,
 ( 4, 4 ),
 ( 0.000000000000000000, 0.0001000000000000028915 ),
 .UNSPECIFIED. ) ;
#5409=CARTESIAN_POINT ( 'NONE',  ( -74.62287095715005592, -24.64898659630367561, 1.056161002820824368 ) ) ;
#5410=CARTESIAN_POINT ( 'NONE',  ( -7.471142097702432316, -20.87072022463130239, 11.49999999999999645 ) ) ;
#5413=CARTESIAN_POINT ( 'NONE',  ( 22.57354875331468591, -1.174960877787051716, 11.49999999999998934 ) ) ;
#5414=CARTESIAN_POINT ( 'NONE',  ( -115.5528638974274003, -24.52399227489127043, 9.353111116836528183 ) ) ;
#5415=ORIENTED_EDGE ( 'NONE', *, *, #52219, .F. ) ;
#5417=ORIENTED_EDGE ( 'NONE', *, *, #64498, .F. ) ;
#5418=CARTESIAN_POINT ( 'NONE',  ( -69.58953762381672448, -23.47593901973091235, -1.443836447539006196 ) ) ;
#5420=CARTESIAN_POINT ( 'NONE',  ( -55.52287095715005449, -25.00158670708909270, 2.256160236439166411 ) ) ;
#5423=CARTESIAN_POINT ( 'NONE',  ( 11.91227609878784399, -18.80521639033699799, -1.500000000000002220 ) ) ;
#5424=CARTESIAN_POINT ( 'NONE',  ( -50.34609605362255280, -25.13941496713000845, 7.561522378954885326 ) ) ;
#5426=CARTESIAN_POINT ( 'NONE',  ( -73.92287095715008149, -23.47596703998600276, 11.44779298504227860 ) ) ;
#5428=CARTESIAN_POINT ( 'NONE',  ( -87.52287095715006160, -23.48786465467241058, 11.44779295918254292 ) ) ;
#5429=CARTESIAN_POINT ( 'NONE',  ( -103.5228709571500758, -23.47596703998600631, 11.44779298504228215 ) ) ;
#5430=B_SPLINE_CURVE_WITH_KNOTS ( 'NONE', 3,
 ( #21900, #67615, #91930, #6693, #13298, #44275 ),
 .UNSPECIFIED., .F., .F.,
 ( 4, 2, 4 ),
 ( 1.570887131794638196E-05, 0.001396322306279760422, 0.002776935741241574537 ),
 .UNSPECIFIED. ) ;
#5433=CARTESIAN_POINT ( 'NONE',  ( 16.17817332762582794, -10.88531698672339942, 11.49999999999998934 ) ) ;
#5434=CARTESIAN_POINT ( 'NONE',  ( -21.25412285906045895, 3.082840150875858054, 11.49999999999998934 ) ) ;
#5436=CARTESIAN_POINT ( 'NONE',  ( -120.5228709571500190, -24.52232992886364471, 0.6492154411906051470 ) ) ;
#5437=CARTESIAN_POINT ( 'NONE',  ( -97.62287095715005592, -29.50250786944525672, 11.44777988621623166 ) ) ;
#5438=CARTESIAN_POINT ( 'NONE',  ( -2.657479817400386413, -22.66247145590962120, -1.500000000000002220 ) ) ;
#5441=CARTESIAN_POINT ( 'NONE',  ( -96.50664446042894440, -24.66019654487199375, 8.947790411086115725 ) ) ;
#5443=CARTESIAN_POINT ( 'NONE',  ( 15.91301918423788919, -12.03417825965012433, 11.49999999999999645 ) ) ;
#5445=AXIS2_PLACEMENT_3D ( 'NONE', #32011, #39118, #560 ) ;
#5446=CARTESIAN_POINT ( 'NONE',  ( -74.60679680638413913, -23.48786465467241058, 11.44779295918254824 ) ) ;
#5447=CARTESIAN_POINT ( 'NONE',  ( -43.62287095715004881, -23.47593901973091235, -1.443836447539011525 ) ) ;
#5448=ADVANCED_FACE ( 'NONE', ( #64705 ), #3784, .T. ) ;
#5449=EDGE_LOOP ( 'NONE', ( #13137, #38982, #72786, #84044 ) ) ;
#5450=CARTESIAN_POINT ( 'NONE',  ( -83.52287095715007581, -24.51387760970724372, 9.387446482453407626 ) ) ;
#5452=CARTESIAN_POINT ( 'NONE',  ( -18.02536786162489335, -12.12045427182966861, -1.500000000000002220 ) ) ;
#5454=CARTESIAN_POINT ( 'NONE',  ( 19.09806219120973125, -4.162641619376711510, -1.500000000000002220 ) ) ;
#5455=CARTESIAN_POINT ( 'NONE',  ( -99.55473692232246208, -25.18616201609388483, 6.774537685832302536 ) ) ;
#5456=VERTEX_POINT ( 'NONE', #43341 ) ;
#5459=CARTESIAN_POINT ( 'NONE',  ( -42.62287095715004881, -29.50250243563736774, 8.947779886222148704 ) ) ;
#5461=CARTESIAN_POINT ( 'NONE',  ( 7.908618202329199320, -18.92053725880622039, 11.49999999999999645 ) ) ;
#5462=DIRECTION ( 'NONE',  ( -3.773278334453079618E-23, 0.9999999999976377785, 2.173523156925979975E-06 ) ) ;
#5463=EDGE_CURVE ( 'NONE', #125, #56501, #75787, .T. ) ;
#5465=B_SPLINE_CURVE_WITH_KNOTS ( 'NONE', 3,
 ( #75075, #59880, #51761, #19297 ),
 .UNSPECIFIED., .F., .F.,
 ( 4, 4 ),
 ( 0.000000000000000000, 9.999999999998897304E-05 ),
 .UNSPECIFIED. ) ;
#5466=ORIENTED_EDGE ( 'NONE', *, *, #87824, .F. ) ;
#5467=CARTESIAN_POINT ( 'NONE',  ( -58.62287095715006302, -24.65952944569304250, 1.056160979905695463 ) ) ;
#5468=CARTESIAN_POINT ( 'NONE',  ( -39.44774024104455634, -25.18431059086297452, 4.157780032001940462 ) ) ;
#5470=ADVANCED_FACE ( 'NONE', ( #88511 ), #34720, .F. ) ;
#5471=FACE_OUTER_BOUND ( 'NONE', #62373, .T. ) ;
#5472=VECTOR ( 'NONE', #96581, 1000.000000000000114 ) ;
#5473=ORIENTED_EDGE ( 'NONE', *, *, #19138, .F. ) ;
#5475=CARTESIAN_POINT ( 'NONE',  ( -16.13607370526515794, 16.44073208242836159, 11.49999999999999645 ) ) ;
#5476=CARTESIAN_POINT ( 'NONE',  ( -21.69093436787670726, -6.948586514802197023, 11.49999999999998934 ) ) ;
#5479=DIRECTION ( 'NONE',  ( -3.773278334453080206E-23, 0.9999999999976377785, 2.173523156925979552E-06 ) ) ;
#5481=DIRECTION ( 'NONE',  ( 0.000000000000000000, 0.9999999999976377785, 2.173523156925979975E-06 ) ) ;
#5482=CARTESIAN_POINT ( 'NONE',  ( -110.6248244526476014, -24.83618233451450763, 1.606449574219537935 ) ) ;
#5483=CARTESIAN_POINT ( 'NONE',  ( 6.492371748702247203, -20.92784845389783399, 11.49999999999998934 ) ) ;
#5484=DIRECTION ( 'NONE',  ( -3.773278334444167608E-23, 1.000000000000000000, 0.000000000000000000 ) ) ;
#5485=PLANE ( 'NONE',  #50298 ) ;
#5488=CARTESIAN_POINT ( 'NONE',  ( -58.49331616262661981, -24.51314013834315020, 0.6176544820404091807 ) ) ;
#5489=VERTEX_POINT ( 'NONE', #81396 ) ;
#5490=CARTESIAN_POINT ( 'NONE',  ( 19.37909195245082472, -6.530858791768283211, 11.49999999999998934 ) ) ;
#5491=ORIENTED_EDGE ( 'NONE', *, *, #29005, .T. ) ;
#5492=ORIENTED_EDGE ( 'NONE', *, *, #12278, .T. ) ;
#5493=ORIENTED_EDGE ( 'NONE', *, *, #56837, .F. ) ;
#5495=EDGE_CURVE ( 'NONE', #44267, #64400, #73777, .T. ) ;
#5496=CARTESIAN_POINT ( 'NONE',  ( 3.314627170985911420, 22.80399709308638023, 11.49999999999998934 ) ) ;
#5497=CARTESIAN_POINT ( 'NONE',  ( -61.50935598288339889, -23.96119346886880308, -0.6495511937832122440 ) ) ;
#5498=CARTESIAN_POINT ( 'NONE',  ( -19.95319933381289701, -3.276446921841525306, -1.500000000000002220 ) ) ;
#5499=ORIENTED_EDGE ( 'NONE', *, *, #71438, .F. ) ;
#5500=CARTESIAN_POINT ( 'NONE',  ( -122.5228709571500758, -23.47593901973090524, -1.443836447538996204 ) ) ;
#5501=CARTESIAN_POINT ( 'NONE',  ( -101.5228709571500758, -23.47593901973090524, -1.443836447538996426 ) ) ;
#5503=CARTESIAN_POINT ( 'NONE',  ( -99.58679885002307230, -24.51419770103158413, 9.386484678747175181 ) ) ;
#5504=CARTESIAN_POINT ( 'NONE',  ( 17.37860173834871347, 12.56526366372364301, 11.49999999999999645 ) ) ;
#5505=ORIENTED_EDGE ( 'NONE', *, *, #65886, .T. ) ;
#5506=FACE_OUTER_BOUND ( 'NONE', #84119, .T. ) ;
#5507=ORIENTED_EDGE ( 'NONE', *, *, #50403, .T. ) ;
#5508=CARTESIAN_POINT ( 'NONE',  ( 4.478411676025833010, -20.21887007069289766, -1.500000000000002220 ) ) ;
#5509=ORIENTED_EDGE ( 'NONE', *, *, #60776, .F. ) ;
#5510=EDGE_CURVE ( 'NONE', #92347, #63576, #38227, .T. ) ;
#5511=CARTESIAN_POINT ( 'NONE',  ( -29.52287095715006160, -24.57685061924431835, 8.947790457046968626 ) ) ;
#5512=ORIENTED_EDGE ( 'NONE', *, *, #57691, .T. ) ;
#5515=CARTESIAN_POINT ( 'NONE',  ( 13.87900837158347755, -15.70065903812341013, -1.500000000000002220 ) ) ;
#5516=CARTESIAN_POINT ( 'NONE',  ( -6.887433846447126307, -20.85920400149894149, 11.49999999999999645 ) ) ;
#5517=CARTESIAN_POINT ( 'NONE',  ( -81.52287095715006160, -23.48786465467241058, 11.44779295918254469 ) ) ;
#5518=CARTESIAN_POINT ( 'NONE',  ( -8.307687032909205627, 20.95097986170506488, -1.500000000000002220 ) ) ;
#5519=B_SPLINE_CURVE_WITH_KNOTS ( 'NONE', 3,
 ( #30719, #82998, #44462, #75386 ),
 .UNSPECIFIED., .F., .F.,
 ( 4, 4 ),
 ( 0.000000000000000000, 9.999999999999592548E-05 ),
 .UNSPECIFIED. ) ;
#5520=CARTESIAN_POINT ( 'NONE',  ( -16.25153318171239647, -13.25006309444557751, 11.49999999999998934 ) ) ;
#5522=CARTESIAN_POINT ( 'NONE',  ( -119.5202022874163532, -23.96169478059714564, 10.65365249895717170 ) ) ;
#5530=CARTESIAN_POINT ( 'NONE',  ( -20.95461191387366284, 4.708766595171775649, -1.500000000000002220 ) ) ;
#5531=CARTESIAN_POINT ( 'NONE',  ( -105.5228709571500616, -24.62285846331440098, 9.038163153548232742 ) ) ;
#5532=ORIENTED_EDGE ( 'NONE', *, *, #72612, .T. ) ;
#5533=CARTESIAN_POINT ( 'NONE',  ( -20.67868931609407213, -4.308284118179648736, -1.500000000000002220 ) ) ;
#5535=CARTESIAN_POINT ( 'NONE',  ( -64.49197637527058191, -24.65952944569304250, 1.056160979905695685 ) ) ;
#5540=CARTESIAN_POINT ( 'NONE',  ( 21.13397978930849064, -6.478279476769641221, -1.500000000000002220 ) ) ;
#5546=EDGE_CURVE ( 'NONE', #84539, #80523, #17994, .T. ) ;
#5547=EDGE_CURVE ( 'NONE', #38515, #76664, #47952, .T. ) ;
#5548=CARTESIAN_POINT ( 'NONE',  ( -58.62287095715004881, -23.47593901973091235, -1.443836447539007972 ) ) ;
#5549=B_SPLINE_CURVE_WITH_KNOTS ( 'NONE', 3,
 ( #76015, #14622, #83126, #68421, #67932, #29349 ),
 .UNSPECIFIED., .F., .F.,
 ( 4, 2, 4 ),
 ( 6.391158118967745954E-06, 0.001387004593080788098, 0.002767618028042608501 ),
 .UNSPECIFIED. ) ;
#5551=CARTESIAN_POINT ( 'NONE',  ( -9.780116039169133302, 16.78644576961053048, -1.500000000000002220 ) ) ;
#5553=CARTESIAN_POINT ( 'NONE',  ( -19.64189229742525455, -8.423329616690555355, -1.500000000000002220 ) ) ;
#5554=CARTESIAN_POINT ( 'NONE',  ( -26.09636659181000340, -24.96935267319560126, 4.940287552382958580 ) ) ;
#5555=CARTESIAN_POINT ( 'NONE',  ( -66.62287095715008434, -24.33832256527048088, 0.1851278514138594566 ) ) ;
#5556=CARTESIAN_POINT ( 'NONE',  ( -0.1426030150137709562, -21.20389190742572083, 11.50200000000000422 ) ) ;
#5557=DIRECTION ( 'NONE',  ( 3.773278334444167608E-23, -1.000000000000000000, 0.000000000000000000 ) ) ;
#5558=CARTESIAN_POINT ( 'NONE',  ( 6.494847429386178206, -21.66115869805930672, -1.500000000000002220 ) ) ;
#5559=B_SPLINE_CURVE_WITH_KNOTS ( 'NONE', 3,
 ( #73898, #11493, #9996, #71914 ),
 .UNSPECIFIED., .F., .F.,
 ( 4, 4 ),
 ( 0.6609719839146940279, 0.6699784151868093396 ),
 .UNSPECIFIED. ) ;
#5560=VERTEX_POINT ( 'NONE', #90004 ) ;
#5561=CARTESIAN_POINT ( 'NONE',  ( -110.5228709571500758, -23.47593901973090524, -1.443836447538996204 ) ) ;
#5563=CARTESIAN_POINT ( 'NONE',  ( 9.697495225759652726, 17.24774500829319734, 11.49999999999999645 ) ) ;
#5564=CARTESIAN_POINT ( 'NONE',  ( -74.55620429048340725, -23.48783264082478439, -1.443836473390066821 ) ) ;
#5566=B_SPLINE_CURVE_WITH_KNOTS ( 'NONE', 3,
 ( #89073, #33274, #42422, #34787 ),
 .UNSPECIFIED., .F., .F.,
 ( 4, 4 ),
 ( 0.3790364612049875181, 0.3800372082457528222 ),
 .UNSPECIFIED. ) ;
#5568=VERTEX_POINT ( 'NONE', #13361 ) ;
#5569=CARTESIAN_POINT ( 'NONE',  ( -66.52287095715006160, -24.64898659630528854, 1.056161002820824368 ) ) ;
#5570=CARTESIAN_POINT ( 'NONE',  ( -29.71166344112055668, -25.26026716537907291, 3.608440118052277157 ) ) ;
#5571=FACE_OUTER_BOUND ( 'NONE', #77902, .T. ) ;
#5572=CARTESIAN_POINT ( 'NONE',  ( 17.58597629297885589, -12.55149374826878272, -1.500000000000002220 ) ) ;
#5573=CARTESIAN_POINT ( 'NONE',  ( -49.88732701573676565, -25.27517896348679827, 2.919594870841833334 ) ) ;
#5574=CARTESIAN_POINT ( 'NONE',  ( -17.02366064725396555, -9.230830265533395362, -1.500000000000002220 ) ) ;
#5577=CARTESIAN_POINT ( 'NONE',  ( -15.51018552496569392, -12.33189742059753868, -1.500000000000002220 ) ) ;
#5578=ORIENTED_EDGE ( 'NONE', *, *, #83070, .T. ) ;
#5579=AXIS2_PLACEMENT_3D ( 'NONE', #4956, #64892, #80579 ) ;
#5580=CARTESIAN_POINT ( 'NONE',  ( -3.904290608643684379, -19.93223805144805283, 11.49999999999999645 ) ) ;
#5582=EDGE_CURVE ( 'NONE', #41241, #34495, #99850, .T. ) ;
#5584=ADVANCED_FACE ( 'NONE', ( #14358 ), #60066, .T. ) ;
#5585=ORIENTED_EDGE ( 'NONE', *, *, #88413, .T. ) ;
#5587=CARTESIAN_POINT ( 'NONE',  ( -30.61333094834725088, -24.36247485673954571, 0.01136689895587403298 ) ) ;
#5588=CARTESIAN_POINT ( 'NONE',  ( -85.62287095715004170, -29.50249982740957577, 7.747779886224967605 ) ) ;
#5589=CARTESIAN_POINT ( 'NONE',  ( -71.52287095715003318, -23.73934037231756022, 11.05740245334328797 ) ) ;
#5591=CARTESIAN_POINT ( 'NONE',  ( -31.52287095715006870, -23.95044443724991368, 10.65354141964649415 ) ) ;
#5592=CARTESIAN_POINT ( 'NONE',  ( -2.827821146493835425, 19.88259668395040691, -1.500000000000002220 ) ) ;
#5593=EDGE_CURVE ( 'NONE', #2529, #79651, #90498, .T. ) ;
#5597=EDGE_CURVE ( 'NONE', #30238, #34031, #58722, .T. ) ;
#5598=CARTESIAN_POINT ( 'NONE',  ( -19.65108876255925807, -11.61119296138784662, 11.49999999999999645 ) ) ;
#5599=CARTESIAN_POINT ( 'NONE',  ( -106.5228709571500900, -23.47593901973090524, -1.443836447538996204 ) ) ;
#5600=LINE ( 'NONE', #20811, #28346 ) ;
#5605=CARTESIAN_POINT ( 'NONE',  ( -3.561414601982806349, 22.15502443119318343, 11.49999999999999645 ) ) ;
#5606=CARTESIAN_POINT ( 'NONE',  ( -50.78074163454362377, -25.29440776045720085, 5.833784451200526355 ) ) ;
#5607=ORIENTED_EDGE ( 'NONE', *, *, #88374, .T. ) ;
#5608=CARTESIAN_POINT ( 'NONE',  ( -16.75749313124890350, -11.57646860041911019, 11.49999999999998934 ) ) ;
#5609=ORIENTED_EDGE ( 'NONE', *, *, #77398, .T. ) ;
#5610=CARTESIAN_POINT ( 'NONE',  ( 17.95915693031428262, 14.28781372813260120, 11.49999999999998934 ) ) ;
#5615=CARTESIAN_POINT ( 'NONE',  ( -77.56400409816168917, -23.48786465467240703, 11.44779295918254647 ) ) ;
#5616=B_SPLINE_CURVE_WITH_KNOTS ( 'NONE', 3,
 ( #86045, #93647, #46488, #94658, #61729, #92648 ),
 .UNSPECIFIED., .F., .F.,
 ( 4, 2, 4 ),
 ( 0.000000000000000000, 0.001380901958385390062, 0.002761803916770780125 ),
 .UNSPECIFIED. ) ;
#5617=CARTESIAN_POINT ( 'NONE',  ( -72.62287095715005592, -23.47593901973091235, -1.443836447539006196 ) ) ;
#5618=CARTESIAN_POINT ( 'NONE',  ( 19.37530031839547107, -8.734557088507903799, 11.49999999999999645 ) ) ;
#5620=ORIENTED_EDGE ( 'NONE', *, *, #39501, .F. ) ;
#5621=CARTESIAN_POINT ( 'NONE',  ( -7.477829544921322125, 20.88912457518834742, -1.500000000000002220 ) ) ;
#5622=CARTESIAN_POINT ( 'NONE',  ( -9.109090448966927767, 18.51201596650851400, 11.49999999999998934 ) ) ;
#5626=CARTESIAN_POINT ( 'NONE',  ( -39.81584396008233284, -25.14432053789888855, 2.967919351947699180 ) ) ;
#5628=ORIENTED_EDGE ( 'NONE', *, *, #6224, .T. ) ;
#5630=CARTESIAN_POINT ( 'NONE',  ( -46.52287095715007581, -24.33832256527048088, 0.1851278514138610942 ) ) ;
#5632=CARTESIAN_POINT ( 'NONE',  ( 1.212613378922696050, -20.72488358683818888, -1.500000000000002220 ) ) ;
#5633=CARTESIAN_POINT ( 'NONE',  ( 7.827691340095081607, 20.28360254610759839, 11.49999999999999645 ) ) ;
#5634=ORIENTED_EDGE ( 'NONE', *, *, #98274, .F. ) ;
#5635=CARTESIAN_POINT ( 'NONE',  ( -40.72474911149932097, -25.27806132187204469, 5.047107969529861293 ) ) ;
#5636=CARTESIAN_POINT ( 'NONE',  ( -113.6228709571500985, -24.51387760970724727, 9.387446482453412955 ) ) ;
#5637=CARTESIAN_POINT ( 'NONE',  ( -115.5183070177505869, -24.15503026093914940, -0.2815557561904543094 ) ) ;
#5638=CARTESIAN_POINT ( 'NONE',  ( 14.18375884139645215, 17.39688726336347102, 11.49999999999998934 ) ) ;
#5639=CARTESIAN_POINT ( 'NONE',  ( -50.80769758106637823, -25.31296745734188036, 4.647238349682671910 ) ) ;
#5640=EDGE_LOOP ( 'NONE', ( #43228, #20314, #41991, #42658 ) ) ;
#5642=CARTESIAN_POINT ( 'NONE',  ( -69.52287095715007581, -24.50321055353803601, 9.387540953477520489 ) ) ;
#5646=CARTESIAN_POINT ( 'NONE',  ( -100.6814946224345846, -25.31401921878175898, 5.197788989978544549 ) ) ;
#5647=ORIENTED_EDGE ( 'NONE', *, *, #2261, .F. ) ;
#5649=CARTESIAN_POINT ( 'NONE',  ( 3.065528897535349628, -21.08962430476942274, -1.500000000000002220 ) ) ;
#5651=CARTESIAN_POINT ( 'NONE',  ( -26.33488822642538452, -24.88201932036028552, 6.524121876823151034 ) ) ;
#5652=CARTESIAN_POINT ( 'NONE',  ( -20.11743356864677423, -6.099313207006018089, 11.49999999999998934 ) ) ;
#5653=FACE_OUTER_BOUND ( 'NONE', #73296, .T. ) ;
#5654=CARTESIAN_POINT ( 'NONE',  ( -6.316168294299441932, 21.79233575779346310, 11.49999999999998934 ) ) ;
#5656=CARTESIAN_POINT ( 'NONE',  ( -29.22287096141859664, -23.36591977638094875, 11.44779298504228038 ) ) ;
#5657=CARTESIAN_POINT ( 'NONE',  ( -14.06357901826416068, -16.81340526219955933, -1.500000000000002220 ) ) ;
#5658=FACE_OUTER_BOUND ( 'NONE', #73987, .T. ) ;
#5659=ORIENTED_EDGE ( 'NONE', *, *, #52191, .F. ) ;
#5660=CARTESIAN_POINT ( 'NONE',  ( -122.5885208564929627, -24.66019654487200086, 8.947790411086113949 ) ) ;
#5662=ADVANCED_FACE ( 'NONE', ( #5760 ), #38464, .T. ) ;
#5663=ORIENTED_EDGE ( 'NONE', *, *, #10316, .T. ) ;
#5665=CARTESIAN_POINT ( 'NONE',  ( -120.5228709571500616, -24.99132157543167310, 2.256160258750667502 ) ) ;
#5666=CARTESIAN_POINT ( 'NONE',  ( -41.62287095715008434, -24.34917612406837861, 0.1852690917426561001 ) ) ;
#5667=ADVANCED_FACE ( 'NONE', ( #16361 ), #46829, .F. ) ;
#5668=CARTESIAN_POINT ( 'NONE',  ( -10.29678027404481000, -22.20953590936370858, -0.9709657327914291702 ) ) ;
#5669=CARTESIAN_POINT ( 'NONE',  ( 20.85495618715548716, -4.085033163991189653, 11.49999999999998934 ) ) ;
#5670=CARTESIAN_POINT ( 'NONE',  ( -112.5526696820402464, -24.34968618360934656, 0.1864209137779000991 ) ) ;
#5671=CARTESIAN_POINT ( 'NONE',  ( -26.71643515402310953, -24.75186064014422982, 2.706679525859190694 ) ) ;
#5673=CARTESIAN_POINT ( 'NONE',  ( -85.59574030132286282, -24.15503026093914229, -0.2815557561904377115 ) ) ;
#5674=CARTESIAN_POINT ( 'NONE',  ( -33.48943877366978938, -24.34968618360933235, 0.1864209137778845560 ) ) ;
#5675=CARTESIAN_POINT ( 'NONE',  ( -79.62287095715005592, -24.33927499327854704, 9.819080762295817166 ) ) ;
#5677=CARTESIAN_POINT ( 'NONE',  ( -3.832734262880480358, 19.25313627021017382, 11.49999999999999645 ) ) ;
#5678=DIRECTION ( 'NONE',  ( -3.773278334453079618E-23, 0.9999999999976377785, 2.173523156925979975E-06 ) ) ;
#5679=CARTESIAN_POINT ( 'NONE',  ( -119.5895376238167103, -23.47593901973091235, -1.443836447538997536 ) ) ;
#5680=EDGE_CURVE ( 'NONE', #90732, #11989, #72034, .T. ) ;
#5681=ORIENTED_EDGE ( 'NONE', *, *, #52529, .T. ) ;
#5683=FACE_OUTER_BOUND ( 'NONE', #72027, .T. ) ;
#5686=CARTESIAN_POINT ( 'NONE',  ( -27.33665423334501554, -24.63129246155760299, 8.218578399534145262 ) ) ;
#5687=CARTESIAN_POINT ( 'NONE',  ( -45.62287095715004881, -24.99132157543083821, 2.256160258750667502 ) ) ;
#5688=CARTESIAN_POINT ( 'NONE',  ( -18.76583335001664565, 6.068782795689376286, 11.49999999999998934 ) ) ;
#5689=ADVANCED_FACE ( 'NONE', ( #93987 ), #24477, .F. ) ;
#5690=VERTEX_POINT ( 'NONE', #2166 ) ;
#5692=PLANE ( 'NONE',  #41551 ) ;
#5695=VERTEX_POINT ( 'NONE', #15356 ) ;
#5698=CARTESIAN_POINT ( 'NONE',  ( -47.53068546992037824, -24.65952944569304606, 1.056160979905696129 ) ) ;
#5701=CARTESIAN_POINT ( 'NONE',  ( -70.15650799851037789, -25.31201593609383593, 5.327550971973213478 ) ) ;
#5702=CARTESIAN_POINT ( 'NONE',  ( -112.5228709571500758, -24.50216790748205042, 0.6166512839542561686 ) ) ;
#5703=CARTESIAN_POINT ( 'NONE',  ( 8.874027960929927517, 17.90919871486395465, -1.500000000000002220 ) ) ;
#5704=EDGE_CURVE ( 'NONE', #89148, #44949, #74315, .T. ) ;
#5705=CARTESIAN_POINT ( 'NONE',  ( -100.4381051993576506, -25.10935037667020708, 2.832404819440808907 ) ) ;
#5706=CARTESIAN_POINT ( 'NONE',  ( -130.5728709571500588, -23.47596703998600631, 11.44779298504227860 ) ) ;
#5710=B_SPLINE_CURVE_WITH_KNOTS ( 'NONE', 3,
 ( #77853, #10233, #18842, #85477, #15464, #56930, #23570, #46928 ),
 .UNSPECIFIED., .F., .F.,
 ( 4, 2, 2, 4 ),
 ( 0.000000000000000000, 0.002001079623178225395, 0.003001619434767336357, 0.004002159246356447320 ),
 .UNSPECIFIED. ) ;
#5712=CARTESIAN_POINT ( 'NONE',  ( -119.5178303131261686, -24.51314013834316086, 0.6176544820404233915 ) ) ;
#5714=CARTESIAN_POINT ( 'NONE',  ( -80.63077793647542535, -24.63419186844610920, 9.035850630976915099 ) ) ;
#5715=FACE_OUTER_BOUND ( 'NONE', #99330, .T. ) ;
#5716=CARTESIAN_POINT ( 'NONE',  ( -81.50938704143565872, -24.15543982623907482, -0.2315651400026469686 ) ) ;
#5717=EDGE_CURVE ( 'NONE', #13954, #52058, #39199, .T. ) ;
#5718=LINE ( 'NONE', #60524, #7560 ) ;
#5719=CARTESIAN_POINT ( 'NONE',  ( -51.61156992512332664, -25.26279989178249963, 4.398685687049794346 ) ) ;
#5720=ORIENTED_EDGE ( 'NONE', *, *, #23048, .F. ) ;
#5721=CARTESIAN_POINT ( 'NONE',  ( -34.62287095715004881, -23.48783264082478084, -1.443836473390074149 ) ) ;
#5722=DIRECTION ( 'NONE',  ( 1.000000000000000000, 3.773278334444166432E-23, 8.201307841325785021E-29 ) ) ;
#5723=ORIENTED_EDGE ( 'NONE', *, *, #78971, .T. ) ;
#5724=CARTESIAN_POINT ( 'NONE',  ( -17.45352675615719917, 10.31968153043333380, 11.49999999999998934 ) ) ;
#5725=CARTESIAN_POINT ( 'NONE',  ( -69.09926072775436978, -25.30615323796089911, 5.508687107256749371 ) ) ;
#5726=DIRECTION ( 'NONE',  ( -3.773278334444167608E-23, 1.000000000000000000, 0.000000000000000000 ) ) ;
#5727=CARTESIAN_POINT ( 'NONE',  ( -82.52287095715007581, -24.66019654487199730, 8.947790411086122830 ) ) ;
#5729=DIRECTION ( 'NONE',  ( 1.000000000000000000, 3.773278334444167608E-23, 8.201307833595939069E-29 ) ) ;
#5730=CARTESIAN_POINT ( 'NONE',  ( -52.52287095715007581, -23.73934037231757088, 11.05740245334329153 ) ) ;
#5731=CARTESIAN_POINT ( 'NONE',  ( 11.77038589110637901, 16.27938679534767275, -1.500000000000002220 ) ) ;
#5732=CARTESIAN_POINT ( 'NONE',  ( -2.639205680565387624, -20.84613592336672028, 11.49999999999999645 ) ) ;
#5733=CARTESIAN_POINT ( 'NONE',  ( -28.74730064801421747, -24.99530720856141741, 7.079464916830322530 ) ) ;
#5734=LINE ( 'NONE', #37186, #70872 ) ;
#5735=CARTESIAN_POINT ( 'NONE',  ( 10.35204687333978057, 19.51823071965408829, -1.500000000000002220 ) ) ;
#5736=VECTOR ( 'NONE', #87338, 1000.000000000000114 ) ;
#5737=CARTESIAN_POINT ( 'NONE',  ( 18.57849760351508195, 8.651319581928444080, -1.500000000000002220 ) ) ;
#5738=CARTESIAN_POINT ( 'NONE',  ( -39.44787993411948435, -25.27805918946292252, 4.218554851849822818 ) ) ;
#5741=PLANE ( 'NONE',  #71995 ) ;
#5742=ORIENTED_EDGE ( 'NONE', *, *, #13121, .F. ) ;
#5744=CARTESIAN_POINT ( 'NONE',  ( -72.55620429048340725, -24.64965694238574656, 8.947790433994198267 ) ) ;
#5748=CARTESIAN_POINT ( 'NONE',  ( -55.52287095715009002, -24.15431212366389246, -0.2830839119429263695 ) ) ;
#5750=CARTESIAN_POINT ( 'NONE',  ( -76.50054984638063615, -24.51314013834316441, 0.6176544820404193947 ) ) ;
#5751=CARTESIAN_POINT ( 'NONE',  ( -16.41017380093149214, -12.48182641202616416, -1.500000000000002220 ) ) ;
#5752=VECTOR ( 'NONE', #21114, 1000.000000000000114 ) ;
#5753=CARTESIAN_POINT ( 'NONE',  ( -11.74548148041400708, 18.04809798412036059, 11.49999999999999645 ) ) ;
#5756=CARTESIAN_POINT ( 'NONE',  ( -129.6228709571500133, -23.48783264082478794, -1.443836473390056607 ) ) ;
#5757=CARTESIAN_POINT ( 'NONE',  ( 8.681249458320607459, -20.60847208623538762, 11.49999999999998934 ) ) ;
#5759=CARTESIAN_POINT ( 'NONE',  ( -80.45048864170028935, -25.12205811578958148, 7.100580275183103751 ) ) ;
#5760=FACE_OUTER_BOUND ( 'NONE', #38086, .T. ) ;
#5763=CARTESIAN_POINT ( 'NONE',  ( -49.59948343357038425, -23.96169478059712432, 10.65365249895718414 ) ) ;
#5764=CARTESIAN_POINT ( 'NONE',  ( 16.07097863352054290, 13.35096362007907622, -1.500000000000002220 ) ) ;
#5766=CARTESIAN_POINT ( 'NONE',  ( -67.59254650884999194, -24.15620529776628800, 10.23563542870660115 ) ) ;
#5770=CARTESIAN_POINT ( 'NONE',  ( 1.363997202867437863, 21.09336101032836908, -1.500000000000002220 ) ) ;
#5777=CARTESIAN_POINT ( 'NONE',  ( -76.62667340351318046, -24.51419770103157347, 9.386484678747176957 ) ) ;
#5779=CARTESIAN_POINT ( 'NONE',  ( -17.45706314325883213, 13.02611496694466275, -1.500000000000002220 ) ) ;
#5780=CARTESIAN_POINT ( 'NONE',  ( -79.45432304757802910, -25.11735646291920077, 7.191156800755474698 ) ) ;
#5781=CARTESIAN_POINT ( 'NONE',  ( 16.98343680692684643, -14.46476453587665389, 11.49999999999999645 ) ) ;
#5785=DIRECTION ( 'NONE',  ( 0.000000000000000000, -2.173523156925980399E-06, 0.9999999999976378895 ) ) ;
#5787=EDGE_CURVE ( 'NONE', #28152, #27902, #96055, .T. ) ;
#5788=EDGE_CURVE ( 'NONE', #29452, #21016, #57437, .T. ) ;
#5790=VERTEX_POINT ( 'NONE', #80780 ) ;
#5791=VECTOR ( 'NONE', #7835, 1000.000000000000114 ) ;
#5792=CARTESIAN_POINT ( 'NONE',  ( -100.4426124108961176, -25.13313949306887451, 7.101635536975466678 ) ) ;
#5793=B_SPLINE_CURVE_WITH_KNOTS ( 'NONE', 3,
 ( #22681, #62790, #38924, #84096 ),
 .UNSPECIFIED., .F., .F.,
 ( 4, 4 ),
 ( 1.387778780781445676E-17, 9.999999999997510880E-05 ),
 .UNSPECIFIED. ) ;
#5796=CARTESIAN_POINT ( 'NONE',  ( -67.58953762381672448, -23.48786465467241058, 11.44779295918254647 ) ) ;
#5797=CARTESIAN_POINT ( 'NONE',  ( 2.021814659504407579E-13, -19.30000000000000426, 11.49999999999998934 ) ) ;
#5798=EDGE_CURVE ( 'NONE', #59154, #36357, #93710, .T. ) ;
#5799=DIRECTION ( 'NONE',  ( -3.773278334453079618E-23, 0.9999999999976377785, 2.173523156925979975E-06 ) ) ;
#5801=CARTESIAN_POINT ( 'NONE',  ( -16.24122463664219396, 10.56255597858309869, 11.49999999999999645 ) ) ;
#5802=DIRECTION ( 'NONE',  ( 0.000000000000000000, 0.9999999999976377785, 2.173523156925979128E-06 ) ) ;
#5803=ORIENTED_EDGE ( 'NONE', *, *, #4430, .T. ) ;
#5806=FACE_OUTER_BOUND ( 'NONE', #80995, .T. ) ;
#5808=B_SPLINE_CURVE_WITH_KNOTS ( 'NONE', 3,
 ( #64141, #19431, #89449, #80334 ),
 .UNSPECIFIED., .F., .F.,
 ( 4, 4 ),
 ( 0.5408862336198214660, 0.5498926648919369997 ),
 .UNSPECIFIED. ) ;
#5809=CARTESIAN_POINT ( 'NONE',  ( 13.00645856128228495, 14.71372164842801844, -1.500000000000002220 ) ) ;
#5810=CARTESIAN_POINT ( 'NONE',  ( -46.62846617042131925, -24.51314013834315020, 0.6176544820404077374 ) ) ;
#5812=CARTESIAN_POINT ( 'NONE',  ( 21.29926025483437257, -3.289820829717503337, -1.500000000000002220 ) ) ;
#5813=CARTESIAN_POINT ( 'NONE',  ( -33.51255700051650877, -23.73791477778911130, 11.05961554403171299 ) ) ;
#5815=PLANE ( 'NONE',  #42768 ) ;
#5817=CARTESIAN_POINT ( 'NONE',  ( 22.99805582222048272, -0.5679727363130141482, -1.500000000000002220 ) ) ;
#5821=LINE ( 'NONE', #6322, #96025 ) ;
#5822=CARTESIAN_POINT ( 'NONE',  ( 17.50376878386636292, -9.983289808088789741, 11.49999999999999645 ) ) ;
#5823=CARTESIAN_POINT ( 'NONE',  ( -108.9756736452620771, -25.28814302825212934, 3.908685561323612667 ) ) ;
#5824=FACE_OUTER_BOUND ( 'NONE', #1681, .T. ) ;
#5830=CARTESIAN_POINT ( 'NONE',  ( -16.51628311069853083, -11.03946451426814690, -1.500000000000002220 ) ) ;
#5832=FACE_OUTER_BOUND ( 'NONE', #7513, .T. ) ;
#5833=CARTESIAN_POINT ( 'NONE',  ( -7.851535696030730982, 18.15458241006858131, -1.500000000000002220 ) ) ;
#5835=CARTESIAN_POINT ( 'NONE',  ( -126.6252828959654693, -23.48786465467241769, 11.44779295918253759 ) ) ;
#5836=B_SPLINE_CURVE_WITH_KNOTS ( 'NONE', 3,
 ( #53391, #5702, #68115, #59503, #84319, #14304 ),
 .UNSPECIFIED., .F., .F.,
 ( 4, 2, 4 ),
 ( 0.000000000000000000, 0.001380764517854767351, 0.002761529035709534702 ),
 .UNSPECIFIED. ) ;
#5840=CARTESIAN_POINT ( 'NONE',  ( -19.40337959798338119, 7.141409694766009508, 11.49999999999999645 ) ) ;
#5841=CARTESIAN_POINT ( 'NONE',  ( -39.53777310077231277, -25.27985545899512587, 5.501674941588943213 ) ) ;
#5842=EDGE_CURVE ( 'NONE', #13993, #38068, #92441, .T. ) ;
#5844=DIRECTION ( 'NONE',  ( -1.000000000000000000, -3.773278334444166432E-23, -8.201307841325785021E-29 ) ) ;
#5845=CARTESIAN_POINT ( 'NONE',  ( 7.379361219544559702, 21.46082085352547963, 11.49999999999999645 ) ) ;
#5846=VERTEX_POINT ( 'NONE', #50831 ) ;
#5847=CARTESIAN_POINT ( 'NONE',  ( -67.52287095715006160, -23.72747288104470087, -1.053458166803226792 ) ) ;
#5849=CARTESIAN_POINT ( 'NONE',  ( -13.64458216870221818, 14.86554040878868044, -1.500000000000002220 ) ) ;
#5851=FACE_OUTER_BOUND ( 'NONE', #83884, .T. ) ;
#5856=CARTESIAN_POINT ( 'NONE',  ( 10.78062712001149492, -20.16176685268226976, -1.500000000000002220 ) ) ;
#5857=CARTESIAN_POINT ( 'NONE',  ( -29.53073231778219210, -24.42996351905146568, 0.6176547996449994749 ) ) ;
#5858=CARTESIAN_POINT ( 'NONE',  ( 18.49883484089910723, -11.16122333755292750, -1.500000000000002220 ) ) ;
#5859=CARTESIAN_POINT ( 'NONE',  ( -123.6259815149813619, -23.73766607897670866, -1.055555164236449350 ) ) ;
#5860=CARTESIAN_POINT ( 'NONE',  ( -65.52287095715006160, -24.15431212366389602, -0.2830839119429243156 ) ) ;
#5861=CARTESIAN_POINT ( 'NONE',  ( 14.20245820080859289, -17.52920931871068433, 11.49999999999999645 ) ) ;
#5862=ORIENTED_EDGE ( 'NONE', *, *, #30640, .F. ) ;
#5863=CARTESIAN_POINT ( 'NONE',  ( -28.37181345154649392, -24.87786573453352901, 2.467876546412420602 ) ) ;
#5864=CARTESIAN_POINT ( 'NONE',  ( 21.52718982488130450, -4.553922534329950089, -1.500000000000002220 ) ) ;
#5865=CARTESIAN_POINT ( 'NONE',  ( -105.5221828483186357, -23.48786465467241769, 11.44779295918254114 ) ) ;
#5866=CARTESIAN_POINT ( 'NONE',  ( -41.16467076663393243, -25.10925807807259247, 3.014416003260400156 ) ) ;
#5871=CARTESIAN_POINT ( 'NONE',  ( -84.62287095715007013, -24.50216790748101303, 0.6166512839513667021 ) ) ;
#5873=B_SPLINE_CURVE_WITH_KNOTS ( 'NONE', 3,
 ( #42568, #57789, #10599, #56800, #72018, #89728, #64423, #57304, #2499, #58288, #95338, #95837, #73504, #18699, #49682, #66415 ),
 .UNSPECIFIED., .F., .F.,
 ( 4, 2, 2, 2, 2, 2, 2, 4 ),
 ( 0.000000000000000000, 0.0001840283733332804216, 0.0003680567466665608431, 0.0007361134933331239631, 0.0009201418666664060381, 0.001104170239999688113, 0.001288198613332970296, 0.001472226986666252263 ),
 .UNSPECIFIED. ) ;
#5874=ORIENTED_EDGE ( 'NONE', *, *, #17942, .T. ) ;
#5876=CARTESIAN_POINT ( 'NONE',  ( -104.5228709571501184, -23.48783264082477373, -1.443836473390087027 ) ) ;
#5877=CARTESIAN_POINT ( 'NONE',  ( -104.6353747070892553, -23.48786465467241413, 11.44779295918254469 ) ) ;
#5878=CARTESIAN_POINT ( 'NONE',  ( 14.97853827808193294, 13.91023239937271860, -1.500000000000002220 ) ) ;
#5883=LINE ( 'NONE', #21592, #59461 ) ;
#5884=CARTESIAN_POINT ( 'NONE',  ( -25.53098197642538736, -24.91566218739149363, 4.942811707542018596 ) ) ;
#5887=CARTESIAN_POINT ( 'NONE',  ( -88.52287095715006160, -23.47593901973090524, -1.443836447538996426 ) ) ;
#5888=CARTESIAN_POINT ( 'NONE',  ( 19.40640353424967302, -7.489167304209242815, 11.49999999999998934 ) ) ;
#5894=ORIENTED_EDGE ( 'NONE', *, *, #16773, .T. ) ;
#5897=CARTESIAN_POINT ( 'NONE',  ( -105.5228709571500758, -23.47596703998600631, 11.44779298504228038 ) ) ;
#5898=EDGE_CURVE ( 'NONE', #6243, #69692, #75554, .T. ) ;
#5899=CARTESIAN_POINT ( 'NONE',  ( -117.7765849230966637, -25.21250125880507653, 3.500947807641612730 ) ) ;
#5902=FACE_OUTER_BOUND ( 'NONE', #61449, .T. ) ;
#5903=CARTESIAN_POINT ( 'NONE',  ( 18.07010470096111021, 12.80550835427630574, 11.49999999999999645 ) ) ;
#5905=CARTESIAN_POINT ( 'NONE',  ( -108.5593186212889520, -23.48783264082478084, -1.443836473390062602 ) ) ;
#5907=CARTESIAN_POINT ( 'NONE',  ( -4.753580043990282888, 22.13494492317406070, 11.49999999999998934 ) ) ;
#5911=EDGE_LOOP ( 'NONE', ( #3431, #44322, #68522, #30830 ) ) ;
#5912=EDGE_CURVE ( 'NONE', #84523, #59400, #79764, .T. ) ;
#5913=VERTEX_POINT ( 'NONE', #87381 ) ;
#5916=CARTESIAN_POINT ( 'NONE',  ( -9.210493908506615313, -17.87979239004878451, 11.49999999999998934 ) ) ;
#5917=DIRECTION ( 'NONE',  ( -3.773278334453079618E-23, 0.9999999999976377785, 2.173523156925978705E-06 ) ) ;
#5919=CARTESIAN_POINT ( 'NONE',  ( -89.52287095715009002, -24.66019654487200441, 8.947790411086119278 ) ) ;
#5920=CARTESIAN_POINT ( 'NONE',  ( 9.404896790668452411, 20.21284700076377305, -1.500000000000002220 ) ) ;
#5921=EDGE_CURVE ( 'NONE', #4897, #50678, #28301, .T. ) ;
#5923=CARTESIAN_POINT ( 'NONE',  ( -78.62287095715005592, -23.47593901973091235, -1.443836447539004642 ) ) ;
#5924=CARTESIAN_POINT ( 'NONE',  ( -81.88534077628074215, -25.23679622552714363, 6.293943003980942308 ) ) ;
#5928=CARTESIAN_POINT ( 'NONE',  ( 7.694069055508638399, 17.95645395709951941, 11.49999999999998934 ) ) ;
#5929=B_SPLINE_CURVE_WITH_KNOTS ( 'NONE', 3,
 ( #35809, #80983, #82472, #81981 ),
 .UNSPECIFIED., .F., .F.,
 ( 4, 4 ),
 ( 0.000000000000000000, 9.999999999998897304E-05 ),
 .UNSPECIFIED. ) ;
#5930=CARTESIAN_POINT ( 'NONE',  ( -20.86232423683148340, -5.086641213604358391, -1.500000000000002220 ) ) ;
#5932=CARTESIAN_POINT ( 'NONE',  ( -120.5228709571500048, -24.92579138211018730, 1.929029949965664015 ) ) ;
#5934=CARTESIAN_POINT ( 'NONE',  ( -6.081610112697643622, 21.96313418072945822, -1.500000000000002220 ) ) ;
#5936=CARTESIAN_POINT ( 'NONE',  ( -96.58651527631003830, -24.51419770103159834, 9.386484678747169852 ) ) ;
#5938=CARTESIAN_POINT ( 'NONE',  ( 4.555139465550277933, 19.45931829295258453, 11.49999999999999645 ) ) ;
#5939=FACE_OUTER_BOUND ( 'NONE', #31744, .T. ) ;
#5940=CARTESIAN_POINT ( 'NONE',  ( -57.52287095715005449, -23.48786465467241058, 11.44779295918254824 ) ) ;
#5942=VERTEX_POINT ( 'NONE', #72173 ) ;
#5945=CARTESIAN_POINT ( 'NONE',  ( -70.62287095715004170, -23.48786465467241058, 11.44779295918254469 ) ) ;
#5946=CARTESIAN_POINT ( 'NONE',  ( -6.878457297428972161, 20.61903435171069532, -1.500000000000002220 ) ) ;
#5948=CARTESIAN_POINT ( 'NONE',  ( 6.425176733589397671, 18.50107501292125178, -1.500000000000002220 ) ) ;
#5949=CARTESIAN_POINT ( 'NONE',  ( -99.29763196087627364, -25.25808875684148092, 6.184470363489280587 ) ) ;
#5953=CARTESIAN_POINT ( 'NONE',  ( -59.62287095715004881, -23.48783264082478794, -1.443836473390069042 ) ) ;
#5955=CARTESIAN_POINT ( 'NONE',  ( 19.38413035786728145, -6.671778716439519030, 11.49999999999999645 ) ) ;
#5959=ORIENTED_EDGE ( 'NONE', *, *, #60356, .F. ) ;
#5965=AXIS2_PLACEMENT_3D ( 'NONE', #67697, #29606, #97623 ) ;
#5966=B_SPLINE_CURVE_WITH_KNOTS ( 'NONE', 3,
 ( #69064, #14764, #52351, #90905 ),
 .UNSPECIFIED., .F., .F.,
 ( 4, 4 ),
 ( 0.03052179486661367805, 0.03952822613872867402 ),
 .UNSPECIFIED. ) ;
#5967=ADVANCED_FACE ( 'NONE', ( #41730 ), #15781, .T. ) ;
#5968=CARTESIAN_POINT ( 'NONE',  ( -85.52287095715004739, -24.83602698348159876, 1.605859176311262182 ) ) ;
#5969=ORIENTED_EDGE ( 'NONE', *, *, #25952, .F. ) ;
#5970=CARTESIAN_POINT ( 'NONE',  ( -119.6228709571500843, -24.34917612406838217, 0.1852690917426684236 ) ) ;
#5971=VECTOR ( 'NONE', #14646, 1000.000000000000114 ) ;
#5972=CARTESIAN_POINT ( 'NONE',  ( -15.77545706029219730, -16.76941864122914083, 11.49999999999999645 ) ) ;
#5973=CARTESIAN_POINT ( 'NONE',  ( -10.92962168092244823, 19.99562239114850826, 11.49999999999998934 ) ) ;
#5976=CARTESIAN_POINT ( 'NONE',  ( -49.56812738534774354, -25.24883509930233672, 3.728933213414787229 ) ) ;
#5977=DIRECTION ( 'NONE',  ( 0.000000000000000000, 2.173523156925980399E-06, -0.9999999999976378895 ) ) ;
#5978=CARTESIAN_POINT ( 'NONE',  ( -110.5878966670114494, -24.73486907724917572, 1.287355809206965240 ) ) ;
#5979=B_SPLINE_CURVE_WITH_KNOTS ( 'NONE', 3,
 ( #31666, #48410, #78332, #717 ),
 .UNSPECIFIED., .F., .F.,
 ( 4, 4 ),
 ( 0.2807004413142643595, 0.2897068725863799488 ),
 .UNSPECIFIED. ) ;
#5980=CARTESIAN_POINT ( 'NONE',  ( 19.28182042344761626, 10.37885539243483812, -1.500000000000002220 ) ) ;
#5983=CARTESIAN_POINT ( 'NONE',  ( -87.60283309997878121, -23.48786465467240703, 11.44779295918254647 ) ) ;
#5984=CARTESIAN_POINT ( 'NONE',  ( -41.45956028061454646, -25.29644670601110690, 4.317464567834644384 ) ) ;
#5985=CARTESIAN_POINT ( 'NONE',  ( -28.62287095715004881, -23.31954350884483773, -1.443835782653508426 ) ) ;
#5987=CARTESIAN_POINT ( 'NONE',  ( -43.62287095715004881, -29.50248528299804818, 1.056150453629031594 ) ) ;
#5988=ORIENTED_EDGE ( 'NONE', *, *, #73110, .T. ) ;
#5989=CARTESIAN_POINT ( 'NONE',  ( 14.97853827808193294, 13.91023239937271860, -1.500000000000002220 ) ) ;
#5993=ORIENTED_EDGE ( 'NONE', *, *, #85675, .F. ) ;
#5994=CARTESIAN_POINT ( 'NONE',  ( 21.63105218614105851, 7.968772182826888262, -1.500000000000002220 ) ) ;
#5995=CARTESIAN_POINT ( 'NONE',  ( -61.52208242660627491, -23.48783264082477018, -1.443836473390096575 ) ) ;
#5996=CARTESIAN_POINT ( 'NONE',  ( -8.208445925564873846, -18.52556626786687488, -1.500000000000002220 ) ) ;
#5997=ORIENTED_EDGE ( 'NONE', *, *, #50163, .T. ) ;
#5999=CARTESIAN_POINT ( 'NONE',  ( -26.09140115595797837, -24.64100662373225603, 2.243760839632586546 ) ) ;
#6000=CARTESIAN_POINT ( 'NONE',  ( -40.93384499162358736, -25.30615997036905185, 5.482420585942463731 ) ) ;
#6001=DIRECTION ( 'NONE',  ( -3.773278334453079030E-23, 0.9999999999976377785, 2.173523156925979128E-06 ) ) ;
#6002=CARTESIAN_POINT ( 'NONE',  ( -99.52218628114583510, -23.48786465467241413, 11.44779295918254469 ) ) ;
#6003=CARTESIAN_POINT ( 'NONE',  ( 2.169945595249806125, 21.32849103866527329, 11.49999999999999645 ) ) ;
#6005=FACE_OUTER_BOUND ( 'NONE', #25921, .T. ) ;
#6006=CARTESIAN_POINT ( 'NONE',  ( -113.5228709571500616, -23.47596703998600631, 11.44779298504228038 ) ) ;
#6007=EDGE_LOOP ( 'NONE', ( #31569, #45963, #76413, #66822 ) ) ;
#6009=CARTESIAN_POINT ( 'NONE',  ( 19.89799572200132971, -5.707369160466581270, -1.500000000000002220 ) ) ;
#6010=ORIENTED_EDGE ( 'NONE', *, *, #48557, .F. ) ;
#6011=CARTESIAN_POINT ( 'NONE',  ( -100.6228709571500559, -23.48786465467241769, 11.44779295918254114 ) ) ;
#6015=CARTESIAN_POINT ( 'NONE',  ( 20.40321384664088811, -4.974606123342796060, -1.500000000000002220 ) ) ;
#6016=EDGE_CURVE ( 'NONE', #84981, #28945, #5296, .T. ) ;
#6017=CARTESIAN_POINT ( 'NONE',  ( 10.07166557822571207, 19.55152498600455857, 11.49999999999999645 ) ) ;
#6018=CARTESIAN_POINT ( 'NONE',  ( -73.55409107130910229, -23.96169478059713143, 10.65365249895718236 ) ) ;
#6019=CARTESIAN_POINT ( 'NONE',  ( 5.070899574700155732, -21.93562493352797915, -1.500000000000002220 ) ) ;
#6020=VECTOR ( 'NONE', #28381, 1000.000000000000114 ) ;
#6021=CARTESIAN_POINT ( 'NONE',  ( -16.25153318171239647, -13.25006309444557751, -1.500000000000002220 ) ) ;
#6022=FACE_OUTER_BOUND ( 'NONE', #13996, .T. ) ;
#6023=B_SPLINE_CURVE_WITH_KNOTS ( 'NONE', 3,
 ( #33772, #35280, #95671, #80946, #26154, #94663, #65743, #65252, #17541, #57128, #58124, #18540, #50496, #95170 ),
 .UNSPECIFIED., .F., .F.,
 ( 4, 2, 2, 2, 2, 2, 4 ),
 ( 0.000000000000000000, 0.0001582106571450110329, 0.0003164213142900220658, 0.0006328426285800532389, 0.0009492639428700843035, 0.001107474600015089699, 0.001265685257160095202 ),
 .UNSPECIFIED. ) ;
#6024=CARTESIAN_POINT ( 'NONE',  ( -119.5185284771687435, -24.35071581493544457, 9.817618358456018157 ) ) ;
#6025=PLANE ( 'NONE',  #68632 ) ;
#6029=ORIENTED_EDGE ( 'NONE', *, *, #45545, .F. ) ;
#6030=EDGE_CURVE ( 'NONE', #100104, #24545, #30821, .T. ) ;
#6031=CARTESIAN_POINT ( 'NONE',  ( -66.59259820813811359, -24.15543982623906771, -0.2315651400026688400 ) ) ;
#6033=CARTESIAN_POINT ( 'NONE',  ( -5.607854029519995898, -20.77141283803394955, -1.500000000000002220 ) ) ;
#6034=PLANE ( 'NONE',  #50527 ) ;
#6036=CARTESIAN_POINT ( 'NONE',  ( -20.79277273739468512, 3.736189789763188607, -1.500000000000002220 ) ) ;
#6039=CARTESIAN_POINT ( 'NONE',  ( -100.5228709571500332, -23.85196035786899316, -0.8779234886475159039 ) ) ;
#6043=CARTESIAN_POINT ( 'NONE',  ( -13.28819421967561532, -17.68372732473523001, -1.500000000000002220 ) ) ;
#6044=CARTESIAN_POINT ( 'NONE',  ( -81.58509740774454144, -24.51419770103159834, 9.386484678747182286 ) ) ;
#6045=EDGE_CURVE ( 'NONE', #40031, #23809, #64638, .T. ) ;
#6046=EDGE_LOOP ( 'NONE', ( #73428, #92760, #90766, #92309 ) ) ;
#6048=CARTESIAN_POINT ( 'NONE',  ( -58.92287095715006018, -23.47596703998600276, 11.44779298504227860 ) ) ;
#6049=FACE_OUTER_BOUND ( 'NONE', #384, .T. ) ;
#6051=CARTESIAN_POINT ( 'NONE',  ( -19.39930850525863804, 0.8904154686948315689, -1.500000000000002220 ) ) ;
#6052=CARTESIAN_POINT ( 'NONE',  ( 3.659817510876246960, 21.07357064420920878, 11.49999999999998934 ) ) ;
#6053=CARTESIAN_POINT ( 'NONE',  ( -69.63554751688641886, -25.07830883915396925, 7.394653300768065485 ) ) ;
#6055=CARTESIAN_POINT ( 'NONE',  ( -79.62287095715005592, -23.48783264082478794, -1.443836473390065489 ) ) ;
#6057=CARTESIAN_POINT ( 'NONE',  ( 8.854694546379761277, 20.84150027139232364, -1.500000000000002220 ) ) ;
#6058=ORIENTED_EDGE ( 'NONE', *, *, #21085, .F. ) ;
#6060=PLANE ( 'NONE',  #21643 ) ;
#6061=CARTESIAN_POINT ( 'NONE',  ( 5.507670110241905448, 19.00313184189250038, 11.49999999999999645 ) ) ;
#6062=CARTESIAN_POINT ( 'NONE',  ( -70.58953762381673869, -25.00182538069145011, 7.747789668545102870 ) ) ;
#6063=B_SPLINE_CURVE_WITH_KNOTS ( 'NONE', 3,
 ( #24688, #17084, #40436, #39429 ),
 .UNSPECIFIED., .F., .F.,
 ( 4, 4 ),
 ( 0.000000000000000000, 9.999999999997510880E-05 ),
 .UNSPECIFIED. ) ;
#6064=PLANE ( 'NONE',  #26915 ) ;
#6065=EDGE_LOOP ( 'NONE', ( #64564, #92466, #78642, #80127 ) ) ;
#6067=CARTESIAN_POINT ( 'NONE',  ( -32.50560602629348494, -29.50248678627064081, 1.747779886239157809 ) ) ;
#6068=CARTESIAN_POINT ( 'NONE',  ( 8.597998336517790108, -19.88058937513707392, 11.49999999999998934 ) ) ;
#6070=CARTESIAN_POINT ( 'NONE',  ( -26.45501174925725962, -24.85202181775033736, 6.809000457855336030 ) ) ;
#6071=CARTESIAN_POINT ( 'NONE',  ( 17.66168439605153395, -8.020940556088177686, -1.500000000000002220 ) ) ;
#6074=CARTESIAN_POINT ( 'NONE',  ( -19.81728208556213389, 0.3677575464312098363, -1.500000000000002220 ) ) ;
#6075=EDGE_CURVE ( 'NONE', #98743, #90405, #87614, .T. ) ;
#6076=B_SPLINE_CURVE_WITH_KNOTS ( 'NONE', 3,
 ( #35522, #5056, #21761, #42644, #21265, #6053, #52735, #11664, #37006, #73579, #4068, #27404, #12162, #43130, #54747, #7555 ),
 .UNSPECIFIED., .F., .F.,
 ( 4, 2, 2, 2, 2, 2, 2, 4 ),
 ( 0.000000000000000000, 0.0002739161793723606311, 0.0005478323587447212623, 0.001095664717489443609, 0.001369580896861805541, 0.001643497076234167690, 0.001917413255606529839, 0.002191329434978891988 ),
 .UNSPECIFIED. ) ;
#6079=CARTESIAN_POINT ( 'NONE',  ( -17.48930418531667996, -10.34094407820366612, 11.49999999999999645 ) ) ;
#6081=EDGE_CURVE ( 'NONE', #91131, #55445, #23416, .T. ) ;
#6084=CARTESIAN_POINT ( 'NONE',  ( -0.05019100999760693627, -22.40023793344692393, 1.063373454495736725 ) ) ;
#6086=LINE ( 'NONE', #4607, #38635 ) ;
#6089=CARTESIAN_POINT ( 'NONE',  ( -14.05898297266747221, -14.31596314050798568, 11.49999999999998934 ) ) ;
#6090=CARTESIAN_POINT ( 'NONE',  ( -120.5895376238167103, -25.00182538069146432, 7.747789668545101094 ) ) ;
#6091=ORIENTED_EDGE ( 'NONE', *, *, #79142, .F. ) ;
#6092=CARTESIAN_POINT ( 'NONE',  ( -117.6228709571500559, -24.64965695001469115, 8.947790433994175174 ) ) ;
#6093=VECTOR ( 'NONE', #6673, 1000.000000000000114 ) ;
#6094=CARTESIAN_POINT ( 'NONE',  ( 9.312063170398973355, -20.82641193498425025, 11.49999999999999645 ) ) ;
#6095=CARTESIAN_POINT ( 'NONE',  ( -49.62307173802614102, -25.26258801428243572, 4.349864120288108538 ) ) ;
#6096=LINE ( 'NONE', #51783, #98006 ) ;
#6097=CARTESIAN_POINT ( 'NONE',  ( -102.6228709571500559, -29.50250243563736774, 8.947779886222138046 ) ) ;
#6099=EDGE_CURVE ( 'NONE', #71512, #65451, #62285, .T. ) ;
#6100=VECTOR ( 'NONE', #35954, 1000.000000000000114 ) ;
#6101=EDGE_CURVE ( 'NONE', #39894, #77573, #64849, .T. ) ;
#6103=DIRECTION ( 'NONE',  ( 0.000000000000000000, 0.9999999999976377785, 2.173523156925979128E-06 ) ) ;
#6104=ORIENTED_EDGE ( 'NONE', *, *, #73379, .F. ) ;
#6105=CARTESIAN_POINT ( 'NONE',  ( -18.95781532540867076, -7.450117396690965066, 11.49999999999998934 ) ) ;
#6106=EDGE_LOOP ( 'NONE', ( #73299, #63937, #16387, #34774 ) ) ;
#6107=CARTESIAN_POINT ( 'NONE',  ( 11.31314246093949727, 19.96360691973900359, -1.500000000000002220 ) ) ;
#6108=PLANE ( 'NONE',  #77642 ) ;
#6110=EDGE_LOOP ( 'NONE', ( #6146, #50049, #56706, #9627 ) ) ;
#6112=EDGE_CURVE ( 'NONE', #82884, #83477, #53836, .T. ) ;
#6113=CARTESIAN_POINT ( 'NONE',  ( -77.55884324271059427, -23.73791477778911840, 11.05961554403170588 ) ) ;
#6114=CARTESIAN_POINT ( 'NONE',  ( -51.58728277246709837, -24.35071581493543036, 9.817618358456028815 ) ) ;
#6115=CARTESIAN_POINT ( 'NONE',  ( -16.96849063341007380, -12.82450338531451450, 11.49999999999999645 ) ) ;
#6116=VERTEX_POINT ( 'NONE', #24738 ) ;
#6118=VERTEX_POINT ( 'NONE', #63841 ) ;
#6119=CARTESIAN_POINT ( 'NONE',  ( 17.16062296631688255, 14.07911611715085876, 11.49999999999998934 ) ) ;
#6120=CARTESIAN_POINT ( 'NONE',  ( -20.60850594246137035, -0.7621957659720622891, 11.49999999999998934 ) ) ;
#6122=ORIENTED_EDGE ( 'NONE', *, *, #27889, .F. ) ;
#6124=CARTESIAN_POINT ( 'NONE',  ( -56.62287095715008434, -24.34917612406837506, 0.1852690917426586537 ) ) ;
#6126=ORIENTED_EDGE ( 'NONE', *, *, #44181, .F. ) ;
#6127=CARTESIAN_POINT ( 'NONE',  ( -125.0508404609613535, -25.24693487555286708, 3.801655821953191960 ) ) ;
#6128=CARTESIAN_POINT ( 'NONE',  ( -41.52884051539315635, -24.66019654487199375, 8.947790411086124607 ) ) ;
#6129=CARTESIAN_POINT ( 'NONE',  ( -130.5728709571500588, -23.50397814795999096, 11.46586199002818418 ) ) ;
#6130=CARTESIAN_POINT ( 'NONE',  ( -20.74012505511919713, -1.853331690952414013, -1.500000000000002220 ) ) ;
#6131=ADVANCED_FACE ( 'NONE', ( #57225 ), #88157, .F. ) ;
#6132=CARTESIAN_POINT ( 'NONE',  ( -21.74948284930419717, -1.071797830193938372, 11.49999999999999645 ) ) ;
#6133=CARTESIAN_POINT ( 'NONE',  ( -51.40810796848847986, -25.09333842084080146, 7.265259977906233679 ) ) ;
#6136=CARTESIAN_POINT ( 'NONE',  ( 14.18375884139645215, 17.39688726336347102, -1.500000000000002220 ) ) ;
#6139=CARTESIAN_POINT ( 'NONE',  ( -71.45307692756523466, -25.31256585376154433, 5.292613253404210738 ) ) ;
#6141=B_SPLINE_SURFACE_WITH_KNOTS ( 'NONE', 3, 1, ( 
 ( #36621, #58976 ),
 ( #20886, #4688 ),
 ( #50865, #27022 ),
 ( #12777, #13273 ),
 ( #28509, #65608 ),
 ( #89915, #19891 ),
 ( #20384, #35636 ),
 ( #82298, #51358 ),
 ( #3693, #96527 ),
 ( #57988, #88926 ),
 ( #19396, #11789 ),
 ( #43746, #97521 ),
 ( #81304, #42759 ),
 ( #74681, #5175 ),
 ( #73692, #81802 ),
 ( #75177, #5671 ),
 ( #67590, #12277 ),
 ( #43255, #98507 ),
 ( #4188, #35141 ),
 ( #66111, #97027 ),
 ( #39116, #62466 ),
 ( #69068, #99004 ),
 ( #83789, #30501 ) ),
 .UNSPECIFIED., .F., .F., .F.,
 ( 4, 1, 1, 1, 1, 1, 1, 1, 1, 1, 1, 1, 1, 1, 1, 1, 1, 1, 1, 1, 4 ),
 ( 2, 2 ),
 ( 0.000000000000000000, 0.06568119799063881770, 0.1284864641740647850, 0.1881751303280078946, 0.2451061306699865161, 0.2994484245294755653, 0.3508229360093824689, 0.3999416805337780434, 0.4466717436323727197, 0.4912545333734983366, 0.5333763442704372304, 0.5738527549682245210, 0.6125263117194527096, 0.6495971364453301256, 0.6855320415538502798, 0.7201057860682015255, 0.7538376629736506240, 0.8189254160467146493, 0.8804934616501651767, 0.9403113338460583615, 1.000000000000000000 ),
 ( 0.000000000000000000, 1.000000000000000000 ),
 .UNSPECIFIED. ) ;
#6142=VERTEX_POINT ( 'NONE', #10521 ) ;
#6143=VERTEX_POINT ( 'NONE', #41481 ) ;
#6145=ADVANCED_FACE ( 'NONE', ( #72437 ), #70075, .T. ) ;
#6146=ORIENTED_EDGE ( 'NONE', *, *, #27326, .F. ) ;
#6147=CARTESIAN_POINT ( 'NONE',  ( 0.1273799443098547757, 21.28700333820561497, -1.500000000000002220 ) ) ;
#6148=EDGE_CURVE ( 'NONE', #64607, #96582, #44131, .T. ) ;
#6149=ORIENTED_EDGE ( 'NONE', *, *, #65294, .F. ) ;
#6151=CARTESIAN_POINT ( 'NONE',  ( -15.31302551872622075, -14.39686070098267479, 11.49999999999998934 ) ) ;
#6155=CARTESIAN_POINT ( 'NONE',  ( 21.59112034314636119, 3.954845139028329015, -1.500000000000002220 ) ) ;
#6157=ORIENTED_EDGE ( 'NONE', *, *, #23504, .T. ) ;
#6158=CARTESIAN_POINT ( 'NONE',  ( -80.53885740889012368, -25.30580248539637012, 4.514386826132675168 ) ) ;
#6159=ADVANCED_FACE ( 'NONE', ( #35861 ), #59474, .T. ) ;
#6163=CARTESIAN_POINT ( 'NONE',  ( -130.5728709571500303, -24.04615231314292600, -0.4716817114508828346 ) ) ;
#6164=CARTESIAN_POINT ( 'NONE',  ( -30.61626505086094951, -24.37935006484465106, 9.703205396196684873 ) ) ;
#6165=CARTESIAN_POINT ( 'NONE',  ( 17.95810460983813783, 11.44545274529666479, -1.500000000000002220 ) ) ;
#6166=CARTESIAN_POINT ( 'NONE',  ( -40.52287095715005449, -25.00158670708908915, 2.256160236439166411 ) ) ;
#6168=B_SPLINE_CURVE_WITH_KNOTS ( 'NONE', 3,
 ( #59384, #75583, #52271, #90326 ),
 .UNSPECIFIED., .F., .F.,
 ( 4, 4 ),
 ( 0.000000000000000000, 9.999999999997510880E-05 ),
 .UNSPECIFIED. ) ;
#6170=VECTOR ( 'NONE', #62550, 1000.000000000000114 ) ;
#6171=CARTESIAN_POINT ( 'NONE',  ( -33.55276516485183436, -23.96119346886880308, -0.6495511937832006977 ) ) ;
#6172=CARTESIAN_POINT ( 'NONE',  ( -20.53624283083718893, 9.024085183690161216, -1.500000000000002220 ) ) ;
#6174=ORIENTED_EDGE ( 'NONE', *, *, #51482, .T. ) ;
#6176=CARTESIAN_POINT ( 'NONE',  ( 19.40334540789412188, 3.064012487144803565, 11.49999999999999645 ) ) ;
#6177=CARTESIAN_POINT ( 'NONE',  ( -99.17877183848689526, -25.29933319754236720, 4.367345793447098501 ) ) ;
#6179=CARTESIAN_POINT ( 'NONE',  ( -89.62287095715004170, -29.50250243563736774, 8.947779886222139822 ) ) ;
#6180=VERTEX_POINT ( 'NONE', #31234 ) ;
#6181=CARTESIAN_POINT ( 'NONE',  ( -88.59160659386742509, -24.15620529776628800, 10.23563542870660115 ) ) ;
#6182=CARTESIAN_POINT ( 'NONE',  ( -42.58953762381672448, -24.64965694238406613, 8.947790433994663672 ) ) ;
#6186=CARTESIAN_POINT ( 'NONE',  ( 2.169241753049089727, -19.58708112974024829, -1.500000000000002220 ) ) ;
#6187=B_SPLINE_CURVE_WITH_KNOTS ( 'NONE', 3,
 ( #54473, #94526, #64110, #2200 ),
 .UNSPECIFIED., .F., .F.,
 ( 4, 4 ),
 ( 0.1788870530518809898, 0.1798878000926463494 ),
 .UNSPECIFIED. ) ;
#6189=ORIENTED_EDGE ( 'NONE', *, *, #62501, .T. ) ;
#6196=CARTESIAN_POINT ( 'NONE',  ( -84.55620429048337883, -23.48783264082478794, -1.443836473390064601 ) ) ;
#6198=CARTESIAN_POINT ( 'NONE',  ( -118.5210660692146547, -23.73766607897671221, -1.055555164236448462 ) ) ;
#6200=CARTESIAN_POINT ( 'NONE',  ( -69.71577706848860601, -25.31201633809909879, 5.512506568089135861 ) ) ;
#6202=CARTESIAN_POINT ( 'NONE',  ( 19.86090765050778728, -2.328952942160339212, -1.500000000000002220 ) ) ;
#6204=CARTESIAN_POINT ( 'NONE',  ( -45.59295858554241221, -24.40133493613049964, 9.663955038902802386 ) ) ;
#6205=ORIENTED_EDGE ( 'NONE', *, *, #57726, .T. ) ;
#6209=DIRECTION ( 'NONE',  ( 0.000000000000000000, 2.173523156925980399E-06, -0.9999999999976378895 ) ) ;
#6210=DIRECTION ( 'NONE',  ( -1.000000000000000000, -3.773278334444167608E-23, -8.201307833595939069E-29 ) ) ;
#6211=CARTESIAN_POINT ( 'NONE',  ( -28.27781825664440873, -24.60093909322488415, 1.715750617954505453 ) ) ;
#6213=EDGE_CURVE ( 'NONE', #18460, #45193, #83519, .T. ) ;
#6214=B_SPLINE_SURFACE_WITH_KNOTS ( 'NONE', 3, 3, ( 
 ( #98398, #11185, #27905, #51245 ),
 ( #42157, #81195, #89805, #58861 ),
 ( #36012, #97900, #4076, #74089 ),
 ( #3585, #82683, #18787, #49766 ),
 ( #57880, #80696, #44135, #27413 ),
 ( #96920, #66987, #57386, #20275 ),
 ( #58372, #35028, #12672, #65500 ) ),
 .UNSPECIFIED., .F., .F., .F.,
 ( 4, 3, 4 ),
 ( 4, 4 ),
 ( 0.0004766839783814931075, 0.1029713700210893451, 0.2054660560637971978 ),
 ( 0.5096236367946838097, 0.5108715007603359393 ),
 .UNSPECIFIED. ) ;
#6217=EDGE_LOOP ( 'NONE', ( #9518, #93130, #1179, #52330 ) ) ;
#6218=CARTESIAN_POINT ( 'NONE',  ( -13.42616926349082895, -15.17935092467416069, 11.49999999999998934 ) ) ;
#6219=CARTESIAN_POINT ( 'NONE',  ( -122.5900856979687603, -24.15543982623907482, -0.2315651400026565443 ) ) ;
#6221=EDGE_CURVE ( 'NONE', #28633, #41093, #56176, .T. ) ;
#6223=CARTESIAN_POINT ( 'NONE',  ( -83.52287095715007581, -23.48783264082477018, -1.443836473390090802 ) ) ;
#6224=EDGE_CURVE ( 'NONE', #69183, #26963, #59767, .T. ) ;
#6228=CARTESIAN_POINT ( 'NONE',  ( -8.609638109768802394, 18.19638482192696216, -1.500000000000002220 ) ) ;
#6229=CARTESIAN_POINT ( 'NONE',  ( 0.3207198112191017025, -21.10926996749724083, 11.49999999999999645 ) ) ;
#6230=EDGE_CURVE ( 'NONE', #28349, #30238, #15008, .T. ) ;
#6231=CARTESIAN_POINT ( 'NONE',  ( -89.81226385320383088, -25.26364009184147008, 3.993462176398974162 ) ) ;
#6232=CARTESIAN_POINT ( 'NONE',  ( 2.303347834742990763, 21.97011321758780866, -1.500000000000002220 ) ) ;
#6233=CARTESIAN_POINT ( 'NONE',  ( -17.34406541665444124, 10.97931167347951842, 11.49999999999998934 ) ) ;
#6237=CARTESIAN_POINT ( 'NONE',  ( -111.5228709571500616, -24.65952944569305316, 1.056160979905704123 ) ) ;
#6240=CARTESIAN_POINT ( 'NONE',  ( -48.87380231474225667, -25.26256937810135028, 6.137091986423513390 ) ) ;
#6243=VERTEX_POINT ( 'NONE', #98747 ) ;
#6247=CARTESIAN_POINT ( 'NONE',  ( 19.39738937107077632, -6.937168198526852514, -1.500000000000002220 ) ) ;
#6248=EDGE_CURVE ( 'NONE', #32532, #58649, #67145, .T. ) ;
#6250=CARTESIAN_POINT ( 'NONE',  ( 14.45009471711328786, 16.04676183837579373, 11.49999999999999645 ) ) ;
#6252=DIRECTION ( 'NONE',  ( -1.000000000000000000, -3.773278334444167608E-23, -8.201307833595939069E-29 ) ) ;
#6253=CARTESIAN_POINT ( 'NONE',  ( -35.58953762381671737, -23.48783264082477729, -1.443836473390072372 ) ) ;
#6254=CARTESIAN_POINT ( 'NONE',  ( 19.81157572017019319, -10.35993776028809421, 11.49999999999998934 ) ) ;
#6255=CARTESIAN_POINT ( 'NONE',  ( -34.52287095715004739, -24.66019654487199730, 8.947790411086121054 ) ) ;
#6256=CARTESIAN_POINT ( 'NONE',  ( -84.55846692228539041, -23.73766607897669445, -1.055555164236457344 ) ) ;
#6257=ORIENTED_EDGE ( 'NONE', *, *, #70402, .T. ) ;
#6259=CARTESIAN_POINT ( 'NONE',  ( -35.57729810147962723, -24.83644354573578994, 8.397322867130093016 ) ) ;
#6261=CARTESIAN_POINT ( 'NONE',  ( 18.75483278694074940, -9.228467059531109129, -1.500000000000002220 ) ) ;
#6262=ORIENTED_EDGE ( 'NONE', *, *, #13583, .F. ) ;
#6263=B_SPLINE_CURVE_WITH_KNOTS ( 'NONE', 3,
 ( #72338, #33258, #34275, #65740 ),
 .UNSPECIFIED., .F., .F.,
 ( 4, 4 ),
 ( 0.1799143969445999580, 0.1889208282167155195 ),
 .UNSPECIFIED. ) ;
#6264=CARTESIAN_POINT ( 'NONE',  ( -86.63220112534330042, -24.15543982623907482, -0.2315651400026493556 ) ) ;
#6265=ADVANCED_FACE ( 'NONE', ( #5902 ), #84021, .F. ) ;
#6266=ORIENTED_EDGE ( 'NONE', *, *, #86906, .F. ) ;
#6267=ORIENTED_EDGE ( 'NONE', *, *, #33647, .T. ) ;
#6268=CARTESIAN_POINT ( 'NONE',  ( -100.5511717382577928, -24.40133493613050319, 9.663955038902802386 ) ) ;
#6269=CARTESIAN_POINT ( 'NONE',  ( -7.596101150008887082, -19.70107428960382734, -1.500000000000002220 ) ) ;
#6271=CARTESIAN_POINT ( 'NONE',  ( -60.58953762381671737, -24.99156044556202261, 7.747789690856174083 ) ) ;
#6272=DIRECTION ( 'NONE',  ( -3.773278334453079618E-23, 0.9999999999976377785, 2.173523156925979975E-06 ) ) ;
#6273=CARTESIAN_POINT ( 'NONE',  ( -17.45706314325883213, 13.02611496694466275, -1.500000000000002220 ) ) ;
#6274=PLANE ( 'NONE',  #57858 ) ;
#6276=CARTESIAN_POINT ( 'NONE',  ( -123.5228709571500616, -29.50248528299804818, 1.056150453629045360 ) ) ;
#6277=CARTESIAN_POINT ( 'NONE',  ( 15.29254711327534899, -15.47666941828629739, -1.500000000000002220 ) ) ;
#6278=CARTESIAN_POINT ( 'NONE',  ( -71.33541886227440898, -25.31639513781093598, 5.089068469391626159 ) ) ;
#6279=CARTESIAN_POINT ( 'NONE',  ( 7.974090105135403839, 20.87195307945309963, 11.49999999999999645 ) ) ;
#6282=CARTESIAN_POINT ( 'NONE',  ( -110.3346797185884327, -25.19502912051678933, 3.293943094755625633 ) ) ;
#6288=EDGE_CURVE ( 'NONE', #45475, #30329, #2988, .T. ) ;
#6289=ORIENTED_EDGE ( 'NONE', *, *, #93198, .T. ) ;
#6290=CARTESIAN_POINT ( 'NONE',  ( -63.52287095715003318, -23.48783264082477018, -1.443836473390091690 ) ) ;
#6291=CARTESIAN_POINT ( 'NONE',  ( 3.302162439418223627, -20.95225242093645690, 11.49999999999998934 ) ) ;
#6292=CARTESIAN_POINT ( 'NONE',  ( -36.62287095715005592, -29.50250786944525672, 11.44777988621624232 ) ) ;
#6293=CARTESIAN_POINT ( 'NONE',  ( -79.20032202190461135, -25.27791825670924553, 6.885559576519126423 ) ) ;
#6294=LINE ( 'NONE', #74799, #11319 ) ;
#6296=CARTESIAN_POINT ( 'NONE',  ( -13.43510958081001050, -13.94331287200543024, -1.500000000000002220 ) ) ;
#6297=ADVANCED_FACE ( 'NONE', ( #76398 ), #85015, .F. ) ;
#6301=CARTESIAN_POINT ( 'NONE',  ( -12.57844902324429448, -14.85176824229388437, 11.49999999999999645 ) ) ;
#6303=AXIS2_PLACEMENT_3D ( 'NONE', #20260, #5048, #19759 ) ;
#6304=B_SPLINE_CURVE_WITH_KNOTS ( 'NONE', 3,
 ( #4784, #35740, #28122, #90019 ),
 .UNSPECIFIED., .F., .F.,
 ( 4, 4 ),
 ( 4.163336342344337027E-17, 9.999999999998898659E-05 ),
 .UNSPECIFIED. ) ;
#6307=CARTESIAN_POINT ( 'NONE',  ( -116.5228709571500616, -23.48786465467241769, 11.44779295918253759 ) ) ;
#6309=B_SPLINE_CURVE_WITH_KNOTS ( 'NONE', 3,
 ( #76945, #837, #53644, #61258 ),
 .UNSPECIFIED., .F., .F.,
 ( 4, 4 ),
 ( 0.000000000000000000, 9.999999999998897304E-05 ),
 .UNSPECIFIED. ) ;
#6310=CARTESIAN_POINT ( 'NONE',  ( -30.62205116524630810, -24.04668586515358442, 10.47594215909545312 ) ) ;
#6311=CARTESIAN_POINT ( 'NONE',  ( 6.560884470684795744, 18.50665934316380756, 11.49999999999998934 ) ) ;
#6314=CARTESIAN_POINT ( 'NONE',  ( -16.67190562677319932, -13.68652177170558204, 11.49999999999998934 ) ) ;
#6315=FACE_OUTER_BOUND ( 'NONE', #16949, .T. ) ;
#6316=CARTESIAN_POINT ( 'NONE',  ( -96.58953762381671027, -23.48783264082478794, -1.443836473390061936 ) ) ;
#6318=CARTESIAN_POINT ( 'NONE',  ( -74.52287095715007581, -23.48786465467241058, 11.44779295918254647 ) ) ;
#6319=CARTESIAN_POINT ( 'NONE',  ( 21.75825945658488436, -7.631246777643061030, -1.500000000000002220 ) ) ;
#6321=LINE ( 'NONE', #37277, #85543 ) ;
#6322=CARTESIAN_POINT ( 'NONE',  ( -105.6228709571500559, -29.50250786944525672, 11.44777988621622988 ) ) ;
#6323=CARTESIAN_POINT ( 'NONE',  ( -19.30929855918770954, 5.666966705251045511, 11.49999999999999645 ) ) ;
#6324=CARTESIAN_POINT ( 'NONE',  ( -84.62287095715008434, -24.33927499327855415, 9.819080762295815390 ) ) ;
#6330=CARTESIAN_POINT ( 'NONE',  ( 18.24224480919323810, -7.949361806615760528, -1.500000000000002220 ) ) ;
#6332=CARTESIAN_POINT ( 'NONE',  ( -18.42202159362721048, -7.168033771007030097, -1.500000000000002220 ) ) ;
#6333=CARTESIAN_POINT ( 'NONE',  ( -42.58702278591343315, -24.34968618360933590, 0.1864209137778841396 ) ) ;
#6335=DIRECTION ( 'NONE',  ( -3.773278334453079030E-23, 0.9999999999976377785, 2.173523156925979128E-06 ) ) ;
#6337=CARTESIAN_POINT ( 'NONE',  ( -19.50335911044312098, -6.847048061534898977, 11.49999999999999645 ) ) ;
#6340=CARTESIAN_POINT ( 'NONE',  ( -109.6228709571500559, -29.50248528299804818, 1.056150453629043584 ) ) ;
#6342=CARTESIAN_POINT ( 'NONE',  ( -22.72798930328562150, -0.2126449523330483371, 11.49999999999999645 ) ) ;
#6343=ORIENTED_EDGE ( 'NONE', *, *, #56463, .F. ) ;
#6344=EDGE_CURVE ( 'NONE', #25080, #79914, #61212, .T. ) ;
#6347=ADVANCED_FACE ( 'NONE', ( #7895 ), #77395, .T. ) ;
#6348=EDGE_CURVE ( 'NONE', #89809, #96286, #98554, .T. ) ;
#6349=CARTESIAN_POINT ( 'NONE',  ( -5.623992922573770592, 19.38241096367466199, -1.500000000000002220 ) ) ;
#6350=CARTESIAN_POINT ( 'NONE',  ( -63.53556326798187825, -24.65952944569304250, 1.056160979905695463 ) ) ;
#6351=B_SPLINE_CURVE_WITH_KNOTS ( 'NONE', 3,
 ( #36152, #44766, #76189, #12794 ),
 .UNSPECIFIED., .F., .F.,
 ( 4, 4 ),
 ( 0.7793352775112003528, 0.7803360245519654903 ),
 .UNSPECIFIED. ) ;
#6353=CARTESIAN_POINT ( 'NONE',  ( -52.52287095715005449, -23.47593901973090524, -1.443836447538997092 ) ) ;
#6354=EDGE_CURVE ( 'NONE', #14971, #65243, #65897, .T. ) ;
#6355=ORIENTED_EDGE ( 'NONE', *, *, #54479, .T. ) ;
#6357=ORIENTED_EDGE ( 'NONE', *, *, #80933, .F. ) ;
#6359=CARTESIAN_POINT ( 'NONE',  ( -9.150087108448493822, 20.98025145036519845, 11.49999999999998934 ) ) ;
#6360=DIRECTION ( 'NONE',  ( -3.773278334453079618E-23, 0.9999999999976377785, 2.173523156925979975E-06 ) ) ;
#6361=CARTESIAN_POINT ( 'NONE',  ( 5.689979955356517571, -20.79666814084963278, -1.500000000000002220 ) ) ;
#6362=CARTESIAN_POINT ( 'NONE',  ( -123.5895128515731329, -24.34968618360933945, 0.1864209137778903291 ) ) ;
#6363=CARTESIAN_POINT ( 'NONE',  ( -34.48977707614956500, -24.34968618360933590, 0.1864209137778841396 ) ) ;
#6364=CARTESIAN_POINT ( 'NONE',  ( -3.950822543831816080, -20.53616823614468956, 11.49999999999999645 ) ) ;
#6365=ORIENTED_EDGE ( 'NONE', *, *, #64617, .F. ) ;
#6366=CARTESIAN_POINT ( 'NONE',  ( -29.11546134910147998, -25.11176486633936022, 3.495844674899231119 ) ) ;
#6367=CARTESIAN_POINT ( 'NONE',  ( 12.33731239738771102, -18.22686410513083288, -1.500000000000002220 ) ) ;
#6368=CARTESIAN_POINT ( 'NONE',  ( -105.6317550840261248, -24.15602025860896163, 10.28564288303535967 ) ) ;
#6369=CARTESIAN_POINT ( 'NONE',  ( -27.68651082257923335, -24.79700317482176786, 7.605672542379497081 ) ) ;
#6371=PLANE ( 'NONE',  #33076 ) ;
#6372=CARTESIAN_POINT ( 'NONE',  ( -90.49972517448894394, -24.92592662359561118, 8.075495903017998245 ) ) ;
#6374=FACE_OUTER_BOUND ( 'NONE', #18385, .T. ) ;
#6375=EDGE_LOOP ( 'NONE', ( #11781, #2174, #49087, #68527 ) ) ;
#6378=CARTESIAN_POINT ( 'NONE',  ( -32.58953762381672448, -24.64898659630367206, 1.056161002820376726 ) ) ;
#6379=DIRECTION ( 'NONE',  ( -3.773278334453079030E-23, 0.9999999999976377785, 2.173523156925979128E-06 ) ) ;
#6380=CARTESIAN_POINT ( 'NONE',  ( -36.65740791118662401, -23.73766607897670156, -1.055555164236459120 ) ) ;
#6381=CARTESIAN_POINT ( 'NONE',  ( 8.549789220347504326, 18.50885834720105905, -1.500000000000002220 ) ) ;
#6386=CARTESIAN_POINT ( 'NONE',  ( -115.6228709571500275, -24.51254535404255464, 9.355368623467647637 ) ) ;
#6388=CARTESIAN_POINT ( 'NONE',  ( -28.52287095715005805, -24.48903441264110015, 8.947790432046794251 ) ) ;
#6390=EDGE_LOOP ( 'NONE', ( #83802, #73561, #23408, #72048 ) ) ;
#6391=DIRECTION ( 'NONE',  ( -3.773278334444166432E-23, 1.000000000000000000, 0.000000000000000000 ) ) ;
#6392=AXIS2_PLACEMENT_3D ( 'NONE', #52293, #68514, #59917 ) ;
#6393=CARTESIAN_POINT ( 'NONE',  ( -29.54485641382474626, -25.26247775934018946, 6.867482800137663546 ) ) ;
#6395=B_SPLINE_CURVE_WITH_KNOTS ( 'NONE', 3,
 ( #44823, #84364, #6741, #83866 ),
 .UNSPECIFIED., .F., .F.,
 ( 4, 4 ),
 ( 0.000000000000000000, 0.0001000000000000028644 ),
 .UNSPECIFIED. ) ;
#6396=CARTESIAN_POINT ( 'NONE',  ( 18.03836333725549324, -10.36167025447706713, -1.500000000000002220 ) ) ;
#6397=ORIENTED_EDGE ( 'NONE', *, *, #60836, .T. ) ;
#6398=DIRECTION ( 'NONE',  ( 3.773278334444166432E-23, -1.000000000000000000, 0.000000000000000000 ) ) ;
#6400=CARTESIAN_POINT ( 'NONE',  ( -107.6228709571500701, -29.50247984919015209, -1.443849546365048253 ) ) ;
#6403=CARTESIAN_POINT ( 'NONE',  ( -65.62287095715005592, -23.48786465467241058, 11.44779295918254647 ) ) ;
#6408=CARTESIAN_POINT ( 'NONE',  ( -51.62287095715005592, -24.65952944569304250, 1.056160979905695019 ) ) ;
#6409=PLANE ( 'NONE',  #12521 ) ;
#6411=CARTESIAN_POINT ( 'NONE',  ( 8.970247382295582383, 20.24485829007567617, 11.49999999999999645 ) ) ;
#6412=ORIENTED_EDGE ( 'NONE', *, *, #66071, .T. ) ;
#6413=CARTESIAN_POINT ( 'NONE',  ( -108.5907138255110880, -24.15543982623907837, -0.2315651400026445539 ) ) ;
#6414=CARTESIAN_POINT ( 'NONE',  ( 22.31954755298990278, 3.869410565987296380, 11.49999999999998934 ) ) ;
#6416=CARTESIAN_POINT ( 'NONE',  ( -27.68651082257923335, -24.79949475646172630, 7.605672536963987262 ) ) ;
#6417=ORIENTED_EDGE ( 'NONE', *, *, #47305, .F. ) ;
#6420=EDGE_CURVE ( 'NONE', #29980, #80353, #80231, .T. ) ;
#6421=CARTESIAN_POINT ( 'NONE',  ( -2.706554608146168217, 19.95013100808389339, -1.500000000000002220 ) ) ;
#6422=B_SPLINE_SURFACE_WITH_KNOTS ( 'NONE', 3, 3, ( 
 ( #11064, #18666, #10063, #72976 ),
 ( #32907, #3466, #87691, #57752 ),
 ( #27291, #94793, #73465, #33900 ),
 ( #3959, #34403, #34903, #25282 ),
 ( #96300, #9558, #95795, #26289 ),
 ( #57265, #50625, #88195, #33392 ),
 ( #58246, #18175, #72474, #17673 ) ),
 .UNSPECIFIED., .F., .F., .F.,
 ( 4, 3, 4 ),
 ( 4, 4 ),
 ( 0.0004766839783842919754, 0.1029713700210908994, 0.2054660560637975031 ),
 ( 0.2795651138368219768, 0.2807068292226991280 ),
 .UNSPECIFIED. ) ;
#6424=ORIENTED_EDGE ( 'NONE', *, *, #24819, .F. ) ;
#6425=LINE ( 'NONE', #99259, #51879 ) ;
#6426=CARTESIAN_POINT ( 'NONE',  ( 13.91197278145025074, 17.48688927191260234, -1.500000000000002220 ) ) ;
#6428=ORIENTED_EDGE ( 'NONE', *, *, #1889, .F. ) ;
#6429=CARTESIAN_POINT ( 'NONE',  ( -101.5468792378191978, -25.25341103933382314, 6.236250660175814531 ) ) ;
#6433=CARTESIAN_POINT ( 'NONE',  ( -37.62287095715005592, -24.64965695001467694, 8.947790433994187609 ) ) ;
#6434=CARTESIAN_POINT ( 'NONE',  ( 8.254404603115069960, -17.72612730319335839, 11.49999999999998934 ) ) ;
#6435=DIRECTION ( 'NONE',  ( 3.773278334444166432E-23, -1.000000000000000000, 0.000000000000000000 ) ) ;
#6436=CARTESIAN_POINT ( 'NONE',  ( -12.84383942963603964, -17.20202612561282862, -1.500000000000002220 ) ) ;
#6441=CARTESIAN_POINT ( 'NONE',  ( -22.32109313027335062, -5.015931025267754251, -1.500000000000002220 ) ) ;
#6443=CARTESIAN_POINT ( 'NONE',  ( -106.5515553243550642, -24.35071581493544457, 9.817618358456019934 ) ) ;
#6445=CARTESIAN_POINT ( 'NONE',  ( 19.86090765050778728, -2.328952942160339212, 11.49999999999999645 ) ) ;
#6447=AXIS2_PLACEMENT_3D ( 'NONE', #93452, #47299, #78225 ) ;
#6448=CARTESIAN_POINT ( 'NONE',  ( -74.59223320385581246, -24.15620529776628800, 10.23563542870659937 ) ) ;
#6450=ORIENTED_EDGE ( 'NONE', *, *, #22098, .F. ) ;
#6453=CARTESIAN_POINT ( 'NONE',  ( -21.72135255055207281, 0.4632500610043824851, -1.500000000000002220 ) ) ;
#6454=CARTESIAN_POINT ( 'NONE',  ( -60.52287095715006160, -25.00158670708908915, 2.256160236439166411 ) ) ;
#6455=VECTOR ( 'NONE', #82406, 1000.000000000000114 ) ;
#6456=CARTESIAN_POINT ( 'NONE',  ( 9.507684299284662188, -17.14340340408069707, -1.500000000000002220 ) ) ;
#6457=CARTESIAN_POINT ( 'NONE',  ( -93.62287095715005592, -29.50250786944525672, 11.44777988621623344 ) ) ;
#6463=CARTESIAN_POINT ( 'NONE',  ( -17.09319154528168383, -11.34935287704045948, 11.49999999999999645 ) ) ;
#6465=CARTESIAN_POINT ( 'NONE',  ( -64.62287095715005592, -29.50248528299804818, 1.056150453629034924 ) ) ;
#6470=CARTESIAN_POINT ( 'NONE',  ( -30.49303573129054357, -23.47596703998576118, 11.44779287168131710 ) ) ;
#6471=CARTESIAN_POINT ( 'NONE',  ( -39.98073487448829155, -25.18430893388618230, 3.395433981284617708 ) ) ;
#6472=CARTESIAN_POINT ( 'NONE',  ( -101.5895376238167103, -23.48783264082479505, -1.443836473390062380 ) ) ;
#6473=EDGE_CURVE ( 'NONE', #60061, #67442, #88690, .T. ) ;
#6474=CARTESIAN_POINT ( 'NONE',  ( -85.52287095715004739, -24.15431212366391023, -0.2830839119429376938 ) ) ;
#6475=EDGE_CURVE ( 'NONE', #76346, #81696, #39846, .T. ) ;
#6476=CARTESIAN_POINT ( 'NONE',  ( -119.6228709571500701, -23.96127896941632685, -0.6493128931037793761 ) ) ;
#6477=EDGE_CURVE ( 'NONE', #23609, #52671, #66955, .T. ) ;
#6478=CARTESIAN_POINT ( 'NONE',  ( 0.1381291366035634904, -23.06709338131901532, 11.49999999999999645 ) ) ;
#6479=CARTESIAN_POINT ( 'NONE',  ( 2.581029390964978187, -22.66945732913600509, -1.500000000000002220 ) ) ;
#6480=CARTESIAN_POINT ( 'NONE',  ( -70.74026866089612042, -25.31517382824369378, 4.894904372083641597 ) ) ;
#6484=DIRECTION ( 'NONE',  ( -3.773278334453079030E-23, 0.9999999999976377785, 2.173523156925979128E-06 ) ) ;
#6486=CARTESIAN_POINT ( 'NONE',  ( -99.19454649804008284, -25.31582273046552700, 5.270710005526405340 ) ) ;
#6487=CARTESIAN_POINT ( 'NONE',  ( -12.72821696145241255, -17.84489267850806726, -1.500000000000002220 ) ) ;
#6488=CARTESIAN_POINT ( 'NONE',  ( -87.62287095715004170, -24.65952944569304606, 1.056160979905700348 ) ) ;
#6489=CARTESIAN_POINT ( 'NONE',  ( -87.54804369446171108, -24.35071581493543391, 9.817618358456025263 ) ) ;
#6490=CARTESIAN_POINT ( 'NONE',  ( -33.52287095715004028, -24.35013146730201683, 9.818937971375110152 ) ) ;
#6491=CARTESIAN_POINT ( 'NONE',  ( -78.62986303001336807, -24.34968618360933945, 0.1864209137778830849 ) ) ;
#6492=CARTESIAN_POINT ( 'NONE',  ( -112.6228709571501128, -24.33832256526968507, 0.1851278514119968077 ) ) ;
#6494=ORIENTED_EDGE ( 'NONE', *, *, #65848, .T. ) ;
#6495=CARTESIAN_POINT ( 'NONE',  ( 14.46511082492616573, -14.46070965572739730, 11.49999999999998934 ) ) ;
#6497=ORIENTED_EDGE ( 'NONE', *, *, #48774, .F. ) ;
#6498=VERTEX_POINT ( 'NONE', #46970 ) ;
#6500=B_SPLINE_CURVE_WITH_KNOTS ( 'NONE', 3,
 ( #83210, #87964, #13696, #44667, #75589, #6092 ),
 .UNSPECIFIED., .F., .F.,
 ( 4, 2, 4 ),
 ( 0.000000000000000000, 0.001380901958385389195, 0.002761803916770778390 ),
 .UNSPECIFIED. ) ;
#6501=CARTESIAN_POINT ( 'NONE',  ( 6.753845092018655016, 22.03294598498517232, -1.500000000000002220 ) ) ;
#6502=CARTESIAN_POINT ( 'NONE',  ( -61.54847807619834299, -24.15543982623907127, -0.2315651400026656481 ) ) ;
#6503=CARTESIAN_POINT ( 'NONE',  ( 19.74221769882431587, -4.499994434135383692, -1.500000000000002220 ) ) ;
#6504=ORIENTED_EDGE ( 'NONE', *, *, #5510, .F. ) ;
#6505=CARTESIAN_POINT ( 'NONE',  ( -54.58953762381672448, -24.64965694238406613, 8.947790433994660120 ) ) ;
#6507=B_SPLINE_CURVE_WITH_KNOTS ( 'NONE', 3,
 ( #53086, #89640, #66826, #12999 ),
 .UNSPECIFIED., .F., .F.,
 ( 4, 4 ),
 ( 0.1388571714212596120, 0.1398579184620250271 ),
 .UNSPECIFIED. ) ;
#6508=CARTESIAN_POINT ( 'NONE',  ( -89.81226385320383088, -25.27880950044345454, 5.947789066509452383 ) ) ;
#6509=CARTESIAN_POINT ( 'NONE',  ( -99.55495890202929843, -23.96169478059713853, 10.65365249895717703 ) ) ;
#6510=CARTESIAN_POINT ( 'NONE',  ( -16.73372362409233105, 13.38858591273363174, 11.49999999999999645 ) ) ;
#6511=VERTEX_POINT ( 'NONE', #34743 ) ;
#6513=CARTESIAN_POINT ( 'NONE',  ( -34.62287095715005592, -23.47593901973091235, -1.443836447539013301 ) ) ;
#6515=CARTESIAN_POINT ( 'NONE',  ( 4.478411676025833010, -20.21887007069289766, 11.49999999999998934 ) ) ;
#6519=CARTESIAN_POINT ( 'NONE',  ( -28.63640793023710174, -24.19694052941946438, 0.1864216068622559508 ) ) ;
#6520=VERTEX_POINT ( 'NONE', #58096 ) ;
#6523=ORIENTED_EDGE ( 'NONE', *, *, #33510, .T. ) ;
#6524=CARTESIAN_POINT ( 'NONE',  ( 20.11839708684271244, 8.774209887332036217, 11.49999999999999645 ) ) ;
#6525=CARTESIAN_POINT ( 'NONE',  ( -73.60155561396484813, -23.73791477778911840, 11.05961554403170766 ) ) ;
#6526=CARTESIAN_POINT ( 'NONE',  ( 15.50834587592193259, -16.38432980155966590, 11.49999999999998934 ) ) ;
#6527=CARTESIAN_POINT ( 'NONE',  ( 0.9685562702117149758, 20.96446713366763248, -1.500000000000002220 ) ) ;
#6528=DIRECTION ( 'NONE',  ( -3.773278334453079030E-23, 0.9999999999976377785, 2.173523156925979128E-06 ) ) ;
#6531=VECTOR ( 'NONE', #62060, 1000.000000000000114 ) ;
#6532=ORIENTED_EDGE ( 'NONE', *, *, #13693, .F. ) ;
#6534=ORIENTED_EDGE ( 'NONE', *, *, #64252, .F. ) ;
#6535=CARTESIAN_POINT ( 'NONE',  ( -66.58776058314595048, -24.34968618360933235, 0.1864209137778773395 ) ) ;
#6538=CARTESIAN_POINT ( 'NONE',  ( -11.74548148041400708, 18.04809798412036059, -1.500000000000002220 ) ) ;
#6539=ADVANCED_FACE ( 'NONE', ( #42378 ), #47409, .T. ) ;
#6540=FACE_OUTER_BOUND ( 'NONE', #44472, .T. ) ;
#6542=CARTESIAN_POINT ( 'NONE',  ( -9.089321149825819290, -19.05894737874082168, 11.49999999999998934 ) ) ;
#6543=CARTESIAN_POINT ( 'NONE',  ( -126.6228709571500843, -24.65952944569305316, 1.056160979905707675 ) ) ;
#6544=CARTESIAN_POINT ( 'NONE',  ( -64.51566560751066959, -23.73766607897670156, -1.055555164236459564 ) ) ;
#6545=PLANE ( 'NONE',  #40525 ) ;
#6546=LINE ( 'NONE', #90783, #28053 ) ;
#6548=CARTESIAN_POINT ( 'NONE',  ( -19.05511597014879044, -11.33806725510066826, -1.500000000000002220 ) ) ;
#6549=CARTESIAN_POINT ( 'NONE',  ( -81.56339976896980204, -23.48786465467241058, 11.44779295918254824 ) ) ;
#6550=VERTEX_POINT ( 'NONE', #50468 ) ;
#6554=CARTESIAN_POINT ( 'NONE',  ( -100.5100558546852341, -24.52300882791530512, 0.6510814631126384810 ) ) ;
#6555=CARTESIAN_POINT ( 'NONE',  ( -12.57844902324429448, -14.85176824229388437, 11.49999999999998934 ) ) ;
#6556=CARTESIAN_POINT ( 'NONE',  ( -21.04715019690976874, -3.721878931196799467, -1.500000000000002220 ) ) ;
#6559=CARTESIAN_POINT ( 'NONE',  ( -40.55620429048338593, -25.00158670708908915, 2.256160236439166855 ) ) ;
#6560=PLANE ( 'NONE',  #33049 ) ;
#6563=CARTESIAN_POINT ( 'NONE',  ( -7.157701736792966507, -21.45640540170154509, -1.500000000000002220 ) ) ;
#6564=ORIENTED_EDGE ( 'NONE', *, *, #70852, .T. ) ;
#6566=CARTESIAN_POINT ( 'NONE',  ( -122.5895376238167245, -23.48783264082479505, -1.443836473390058828 ) ) ;
#6567=CARTESIAN_POINT ( 'NONE',  ( 18.24360591643979035, -7.691401616277519615, 11.49999999999999645 ) ) ;
#6568=CARTESIAN_POINT ( 'NONE',  ( -47.52287095715006160, -29.50247984919015209, -1.443849546365058689 ) ) ;
#6572=CARTESIAN_POINT ( 'NONE',  ( 21.56569437331729233, -1.927008741106717604, -1.500000000000002220 ) ) ;
#6573=CARTESIAN_POINT ( 'NONE',  ( -26.38942647803707686, -24.86721634236063849, 6.669030906457092733 ) ) ;
#6574=CARTESIAN_POINT ( 'NONE',  ( 4.312616920666290987, -18.91975033782923887, -1.500000000000002220 ) ) ;
#6575=PLANE ( 'NONE',  #50723 ) ;
#6576=CARTESIAN_POINT ( 'NONE',  ( -8.418173371947181849, -17.93405594323863284, -1.500000000000002220 ) ) ;
#6577=VERTEX_POINT ( 'NONE', #20008 ) ;
#6578=B_SPLINE_CURVE_WITH_KNOTS ( 'NONE', 3,
 ( #43457, #51566, #4888, #12980, #35833, #43945, #67292, #98212 ),
 .UNSPECIFIED., .F., .F.,
 ( 4, 2, 2, 4 ),
 ( -0.001240666984355836069, -0.0002401179793394933766, 0.0007604310256768488825, 0.002761529035709529498 ),
 .UNSPECIFIED. ) ;
#6579=CARTESIAN_POINT ( 'NONE',  ( -15.63206872509828571, 12.99414084278249071, 11.49999999999999645 ) ) ;
#6580=CARTESIAN_POINT ( 'NONE',  ( -80.49262340036909791, -25.00158670708910691, 2.256160236439221034 ) ) ;
#6581=VECTOR ( 'NONE', #37225, 1000.000000000000114 ) ;
#6584=CARTESIAN_POINT ( 'NONE',  ( -102.5955360307746531, -23.73791477778911840, 11.05961554403170410 ) ) ;
#6585=CARTESIAN_POINT ( 'NONE',  ( -95.52287095715006160, -24.82576562948887400, 8.398263436605493126 ) ) ;
#6587=CARTESIAN_POINT ( 'NONE',  ( -95.62287095715008434, -24.63287334234179582, 0.9662140553045412972 ) ) ;
#6588=CARTESIAN_POINT ( 'NONE',  ( -36.52287095715006870, -29.50248528299804818, 1.056150453629031594 ) ) ;
#6589=CARTESIAN_POINT ( 'NONE',  ( -10.05502934987021391, 17.38067806581081598, 11.49999999999998934 ) ) ;
#6590=CARTESIAN_POINT ( 'NONE',  ( -85.52287095715007581, -24.51163499207180507, 0.6490370598555504911 ) ) ;
#6593=CARTESIAN_POINT ( 'NONE',  ( -130.5728709571500588, -23.56000036390796737, 11.50200000000000244 ) ) ;
#6594=B_SPLINE_CURVE_WITH_KNOTS ( 'NONE', 3,
 ( #17775, #95393, #96391, #42130, #81166, #56855, #26385, #80667, #73560, #57355 ),
 .UNSPECIFIED., .F., .F.,
 ( 4, 2, 2, 2, 4 ),
 ( 0.000000000000000000, 0.0004025782241721760006, 0.0008051564483443520012, 0.001207734672516527948, 0.001610312896688704002 ),
 .UNSPECIFIED. ) ;
#6595=AXIS2_PLACEMENT_3D ( 'NONE', #86539, #77909, #61723 ) ;
#6596=CARTESIAN_POINT ( 'NONE',  ( -20.58715743568940226, -9.973749938417524774, 11.49999999999999645 ) ) ;
#6597=CARTESIAN_POINT ( 'NONE',  ( -102.5228709571500900, -23.47593901973090524, -1.443836447538996648 ) ) ;
#6598=EDGE_CURVE ( 'NONE', #85004, #51581, #68200, .T. ) ;
#6600=FACE_OUTER_BOUND ( 'NONE', #32604, .T. ) ;
#6601=VECTOR ( 'NONE', #34344, 1000.000000000000114 ) ;
#6602=EDGE_CURVE ( 'NONE', #40297, #86774, #17327, .T. ) ;
#6607=CARTESIAN_POINT ( 'NONE',  ( 20.12614038868121824, 2.982395457389826809, -1.500000000000002220 ) ) ;
#6610=CARTESIAN_POINT ( 'NONE',  ( 3.929728083993185184, -22.62717521373229701, 11.49999999999998934 ) ) ;
#6611=PLANE ( 'NONE',  #6392 ) ;
#6613=CARTESIAN_POINT ( 'NONE',  ( -101.5292794699970642, -25.23690811000786383, 6.294209816776285216 ) ) ;
#6614=CARTESIAN_POINT ( 'NONE',  ( -77.58953762381673869, -24.64965694238406968, 8.947790433994654791 ) ) ;
#6615=B_SPLINE_CURVE_WITH_KNOTS ( 'NONE', 3,
 ( #30879, #40502, #23756, #86663, #61845, #71456 ),
 .UNSPECIFIED., .F., .F.,
 ( 4, 2, 4 ),
 ( 0.000000000000000000, 0.001380901958385379220, 0.002761803916770758441 ),
 .UNSPECIFIED. ) ;
#6616=CARTESIAN_POINT ( 'NONE',  ( -111.5228709571500616, -24.64965694238407323, 8.947790433994192938 ) ) ;
#6617=CARTESIAN_POINT ( 'NONE',  ( 21.23515499356076930, 0.7789969333488580006, 11.49999999999999645 ) ) ;
#6618=ORIENTED_EDGE ( 'NONE', *, *, #65677, .F. ) ;
#6620=CARTESIAN_POINT ( 'NONE',  ( 21.60277357391871433, -5.133695162202882578, -1.500000000000002220 ) ) ;
#6621=CARTESIAN_POINT ( 'NONE',  ( -16.38011734009650411, 12.53836025512309149, 11.49999999999998934 ) ) ;
#6622=B_SPLINE_CURVE_WITH_KNOTS ( 'NONE', 3,
 ( #54324, #8640, #39584, #46707 ),
 .UNSPECIFIED., .F., .F.,
 ( 4, 4 ),
 ( 0.1406003993035798150, 0.1496068305756953765 ),
 .UNSPECIFIED. ) ;
#6623=EDGE_LOOP ( 'NONE', ( #73423, #6029, #97349, #91716 ) ) ;
#6624=ORIENTED_EDGE ( 'NONE', *, *, #34997, .F. ) ;
#6625=FACE_OUTER_BOUND ( 'NONE', #25238, .T. ) ;
#6627=ORIENTED_EDGE ( 'NONE', *, *, #36268, .F. ) ;
#6629=CARTESIAN_POINT ( 'NONE',  ( -49.52287095715006870, -23.72773821059535848, 11.05748984161097681 ) ) ;
#6630=CARTESIAN_POINT ( 'NONE',  ( -29.24636659181000198, -25.21267509515801564, 4.940287023516041209 ) ) ;
#6631=CARTESIAN_POINT ( 'NONE',  ( -10.15938669249390180, 18.18672505111813464, -1.500000000000002220 ) ) ;
#6632=CARTESIAN_POINT ( 'NONE',  ( -1.534710021792092594, -21.76038796025502009, 11.49999999999999645 ) ) ;
#6633=CARTESIAN_POINT ( 'NONE',  ( -39.85957971240202369, -25.20729891577929394, 3.457629610838235834 ) ) ;
#6634=CARTESIAN_POINT ( 'NONE',  ( -78.58811849685578466, -24.35071581493543391, 9.817618358456027039 ) ) ;
#6635=CARTESIAN_POINT ( 'NONE',  ( 16.82713599508461400, -14.87465808564757808, 11.49999999999998934 ) ) ;
#6636=CARTESIAN_POINT ( 'NONE',  ( -50.95636528269795207, -25.26334713686265943, 4.561343367844973962 ) ) ;
#6637=EDGE_CURVE ( 'NONE', #58964, #52078, #27042, .T. ) ;
#6638=ORIENTED_EDGE ( 'NONE', *, *, #47320, .T. ) ;
#6643=AXIS2_PLACEMENT_3D ( 'NONE', #69206, #100120, #30641 ) ;
#6644=CARTESIAN_POINT ( 'NONE',  ( -46.50016940544900024, -24.15620529776627379, 10.23563542870660825 ) ) ;
#6646=ORIENTED_EDGE ( 'NONE', *, *, #18955, .T. ) ;
#6647=CARTESIAN_POINT ( 'NONE',  ( 8.224165413489119558, 19.69228431130148493, -1.500000000000002220 ) ) ;
#6650=CARTESIAN_POINT ( 'NONE',  ( -20.98013922110768448, -1.350454208470041273, -1.500000000000002220 ) ) ;
#6651=CARTESIAN_POINT ( 'NONE',  ( -30.50823467185977833, -24.04845685762501617, -0.4713115009884517037 ) ) ;
#6652=CARTESIAN_POINT ( 'NONE',  ( -100.3258897876286255, -25.18527973888543769, 3.296414269619829973 ) ) ;
#6653=LINE ( 'NONE', #37609, #23878 ) ;
#6654=CARTESIAN_POINT ( 'NONE',  ( -8.017166757594178961, 20.41873492177044724, -1.500000000000002220 ) ) ;
#6655=DIRECTION ( 'NONE',  ( -3.773278334453079030E-23, 0.9999999999976377785, 2.173523156925979128E-06 ) ) ;
#6656=VERTEX_POINT ( 'NONE', #51967 ) ;
#6658=B_SPLINE_CURVE_WITH_KNOTS ( 'NONE', 3,
 ( #32119, #94018, #39230, #47860, #46853, #70187, #94520, #671, #17904, #79792, #16897, #31618, #62583, #86410, #93009, #24504 ),
 .UNSPECIFIED., .F., .F.,
 ( 4, 2, 2, 2, 2, 2, 2, 4 ),
 ( 3.496446946337351263E-18, 0.0002171278225386873725, 0.0004342556450773712214, 0.0008685112901547389734, 0.001737022580309472743, 0.002171278225386841579, 0.002605533870464210415, 0.003474045160618947220 ),
 .UNSPECIFIED. ) ;
#6661=CARTESIAN_POINT ( 'NONE',  ( -128.5228709571501611, -23.96127896942151736, -0.6493128930935507803 ) ) ;
#6662=CARTESIAN_POINT ( 'NONE',  ( -30.58080440576787851, -25.30589263001944644, 6.147794833475635379 ) ) ;
#6663=CARTESIAN_POINT ( 'NONE',  ( 20.49606604269246546, -5.804284187783010474, 11.49999999999998934 ) ) ;
#6665=CARTESIAN_POINT ( 'NONE',  ( -51.62287095715005592, -23.47596703998600631, 11.44779298504227505 ) ) ;
#6667=B_SPLINE_CURVE_WITH_KNOTS ( 'NONE', 3,
 ( #41423, #57166, #17579, #56161, #1864, #17075, #94701, #33808, #87089, #28068, #48550, #64790, #81849, #88104, #19938, #36177, #4730, #66656 ),
 .UNSPECIFIED., .F., .F.,
 ( 4, 2, 2, 2, 2, 2, 2, 2, 4 ),
 ( 0.000000000000000000, 0.0002152204991354002641, 0.0004304409982708005283, 0.0008608819965415918408, 0.001291322994812383208, 0.001721763993083174574, 0.002582645989624761211, 0.003013086987895555180, 0.003443527986166349149 ),
 .UNSPECIFIED. ) ;
#6668=CARTESIAN_POINT ( 'NONE',  ( -33.63539978109197648, -24.34968618360933235, 0.1864209137778845560 ) ) ;
#6670=CARTESIAN_POINT ( 'NONE',  ( -11.43049785330379997, -19.34545768653811493, -1.500000000000002220 ) ) ;
#6673=DIRECTION ( 'NONE',  ( -3.773278334453079618E-23, 0.9999999999976377785, 2.173523156925979975E-06 ) ) ;
#6674=CARTESIAN_POINT ( 'NONE',  ( 16.84789977498956404, 10.09486508543780481, 11.49999999999999645 ) ) ;
#6675=CARTESIAN_POINT ( 'NONE',  ( -125.6228709571500275, -23.85196035786900381, -0.8779234886475003607 ) ) ;
#6676=CARTESIAN_POINT ( 'NONE',  ( -82.52287095715003318, -23.96127896942135393, -0.6493128930938705246 ) ) ;
#6677=B_SPLINE_CURVE_WITH_KNOTS ( 'NONE', 3,
 ( #98077, #99566, #91469, #91974, #81875, #59047, #43325, #66682 ),
 .UNSPECIFIED., .F., .F.,
 ( 4, 2, 2, 4 ),
 ( 6.391158118955260688E-06, 0.002007136338672914442, 0.003007508928949895622, 0.004007881519226877236 ),
 .UNSPECIFIED. ) ;
#6679=CARTESIAN_POINT ( 'NONE',  ( -88.52215618628163440, -23.48786465467241413, 11.44779295918254469 ) ) ;
#6680=CARTESIAN_POINT ( 'NONE',  ( -46.52287095715006160, -29.50248528299804818, 1.056150453629033370 ) ) ;
#6681=EDGE_CURVE ( 'NONE', #92149, #93833, #59587, .T. ) ;
#6683=CARTESIAN_POINT ( 'NONE',  ( -25.63684490523837667, -24.87290554392149744, 6.232310010065051920 ) ) ;
#6684=B_SPLINE_CURVE_WITH_KNOTS ( 'NONE', 3,
 ( #19473, #44328, #81383, #20965 ),
 .UNSPECIFIED., .F., .F.,
 ( 4, 4 ),
 ( 0.4908505043302913151, 0.4998569356024067378 ),
 .UNSPECIFIED. ) ;
#6685=B_SPLINE_CURVE_WITH_KNOTS ( 'NONE', 3,
 ( #22146, #99281, #13542, #92665 ),
 .UNSPECIFIED., .F., .F.,
 ( 4, 4 ),
 ( 0.000000000000000000, 0.0001002978970080590907 ),
 .UNSPECIFIED. ) ;
#6686=CARTESIAN_POINT ( 'NONE',  ( 7.987771016649366729, -18.01272016045900415, 11.49999999999998934 ) ) ;
#6687=VERTEX_POINT ( 'NONE', #28623 ) ;
#6688=FACE_OUTER_BOUND ( 'NONE', #67206, .T. ) ;
#6689=FACE_OUTER_BOUND ( 'NONE', #94365, .T. ) ;
#6691=VERTEX_POINT ( 'NONE', #52465 ) ;
#6692=CARTESIAN_POINT ( 'NONE',  ( -96.62287095715005592, -24.64898659630368272, 1.056161002820829697 ) ) ;
#6693=CARTESIAN_POINT ( 'NONE',  ( -103.6228709571500701, -23.96177878511308990, 10.65340807706329862 ) ) ;
#6694=CARTESIAN_POINT ( 'NONE',  ( -55.50250315067101070, -24.15503026093912808, -0.2815557561904589168 ) ) ;
#6695=CARTESIAN_POINT ( 'NONE',  ( -99.09546795806416242, -25.03145021834298234, 6.840688129798706996 ) ) ;
#6697=CARTESIAN_POINT ( 'NONE',  ( -69.64006105340874342, -25.31201646985301323, 5.573124239722496931 ) ) ;
#6699=CARTESIAN_POINT ( 'NONE',  ( -19.24466553037914807, -5.328869878250761971, 11.49999999999998934 ) ) ;
#6700=ADVANCED_FACE ( 'NONE', ( #98620 ), #44082, .T. ) ;
#6701=PLANE ( 'NONE',  #100161 ) ;
#6702=CARTESIAN_POINT ( 'NONE',  ( -45.52798018843675010, -24.83644354573577928, 8.397322867130094792 ) ) ;
#6704=CARTESIAN_POINT ( 'NONE',  ( -119.5193685554757792, -24.15543982623907837, -0.2315651400026547124 ) ) ;
#6705=CARTESIAN_POINT ( 'NONE',  ( -80.58710785548036881, -24.63419186844610920, 9.035850630976915099 ) ) ;
#6706=EDGE_CURVE ( 'NONE', #11463, #24959, #57261, .T. ) ;
#6707=CARTESIAN_POINT ( 'NONE',  ( -124.7734026561379466, -25.27150408776893542, 5.922772873374069214 ) ) ;
#6708=CARTESIAN_POINT ( 'NONE',  ( -39.52824657088962823, -24.65952944569304250, 1.056160979905697017 ) ) ;
#6711=CARTESIAN_POINT ( 'NONE',  ( -119.6228709571500559, -24.64898659630368627, 1.056161002820833028 ) ) ;
#6712=CARTESIAN_POINT ( 'NONE',  ( -51.44554956638231147, -25.31574398867087439, 4.646412717996129871 ) ) ;
#6715=ORIENTED_EDGE ( 'NONE', *, *, #19735, .F. ) ;
#6716=CARTESIAN_POINT ( 'NONE',  ( -18.19507518397214341, 8.946258903265221107, -1.500000000000002220 ) ) ;
#6719=FACE_OUTER_BOUND ( 'NONE', #29940, .T. ) ;
#6722=CARTESIAN_POINT ( 'NONE',  ( -94.62287095715005592, -23.47596703998600631, 11.44779298504227860 ) ) ;
#6724=AXIS2_PLACEMENT_3D ( 'NONE', #87710, #17694, #71494 ) ;
#6725=CARTESIAN_POINT ( 'NONE',  ( 18.53703574427524359, 7.882278514257341051, -1.500000000000002220 ) ) ;
#6726=CARTESIAN_POINT ( 'NONE',  ( 3.661087877195506213, -20.73962600213626217, 11.49999999999999645 ) ) ;
#6728=CARTESIAN_POINT ( 'NONE',  ( -118.5562042904833930, -24.65952944569305316, 1.056160979905707009 ) ) ;
#6729=CARTESIAN_POINT ( 'NONE',  ( 21.13397978930849064, -6.478279476769641221, -1.500000000000002220 ) ) ;
#6730=CARTESIAN_POINT ( 'NONE',  ( -1.764913036440812322, 20.45846032914734280, -1.500000000000002220 ) ) ;
#6731=CARTESIAN_POINT ( 'NONE',  ( -93.62287095715007013, -23.47596703998600631, 11.44779298504227860 ) ) ;
#6733=ORIENTED_EDGE ( 'NONE', *, *, #4640, .F. ) ;
#6737=LINE ( 'NONE', #37691, #77703 ) ;
#6738=VERTEX_POINT ( 'NONE', #1676 ) ;
#6739=ORIENTED_EDGE ( 'NONE', *, *, #93642, .T. ) ;
#6740=ORIENTED_EDGE ( 'NONE', *, *, #52915, .F. ) ;
#6741=CARTESIAN_POINT ( 'NONE',  ( -65.55620429048337883, -23.48783264082478439, -1.443836473390067487 ) ) ;
#6742=CARTESIAN_POINT ( 'NONE',  ( -49.52287095715007581, -23.47593901973090169, -1.443836447538997092 ) ) ;
#6743=CARTESIAN_POINT ( 'NONE',  ( -68.51606030823643323, -23.73791477778911840, 11.05961554403170943 ) ) ;
#6744=CARTESIAN_POINT ( 'NONE',  ( 19.46067915675286386, 6.892634557253153105, -1.500000000000002220 ) ) ;
#6745=CARTESIAN_POINT ( 'NONE',  ( -9.004746288917990782, -19.65190454534591069, 11.49999999999999645 ) ) ;
#6747=FACE_OUTER_BOUND ( 'NONE', #34614, .T. ) ;
#6748=CARTESIAN_POINT ( 'NONE',  ( -57.62287095715005592, -24.33927499327854704, 9.819080762295820719 ) ) ;
#6749=CARTESIAN_POINT ( 'NONE',  ( -21.90463088927077706, -4.570550247397807908, 11.49999999999998934 ) ) ;
#6751=CARTESIAN_POINT ( 'NONE',  ( -84.59926806605869842, -23.73766607897669445, -1.055555164236457566 ) ) ;
#6752=EDGE_LOOP ( 'NONE', ( #10330, #97503, #47451, #94443 ) ) ;
#6755=CARTESIAN_POINT ( 'NONE',  ( 20.33208665566141704, 4.825383418962623239, -1.500000000000002220 ) ) ;
#6756=ORIENTED_EDGE ( 'NONE', *, *, #61276, .F. ) ;
#6757=CARTESIAN_POINT ( 'NONE',  ( -67.63597399538805632, -24.15620529776628800, 10.23563542870660115 ) ) ;
#6758=EDGE_LOOP ( 'NONE', ( #13345, #94360, #40559, #91126 ) ) ;
#6760=EDGE_CURVE ( 'NONE', #35231, #25716, #29365, .T. ) ;
#6761=CARTESIAN_POINT ( 'NONE',  ( -109.5865558906285600, -24.66019654487200441, 8.947790411086113949 ) ) ;
#6762=CARTESIAN_POINT ( 'NONE',  ( 7.804836024166685426, 19.70032748343534834, -1.500000000000002220 ) ) ;
#6763=ORIENTED_EDGE ( 'NONE', *, *, #99474, .F. ) ;
#6765=CARTESIAN_POINT ( 'NONE',  ( -99.61078991697702634, -25.12215613712814744, 6.818453781472685549 ) ) ;
#6766=CARTESIAN_POINT ( 'NONE',  ( -12.70408864715453667, 17.69581422525067183, -1.500000000000002220 ) ) ;
#6768=CARTESIAN_POINT ( 'NONE',  ( -36.62287095715005592, -24.64898659630367916, 1.056161002820819261 ) ) ;
#6769=CARTESIAN_POINT ( 'NONE',  ( -95.52287095715006160, -25.00158670708909980, 2.256160236439166411 ) ) ;
#6770=CARTESIAN_POINT ( 'NONE',  ( -6.878457297428972161, 20.61903435171069532, -1.500000000000002220 ) ) ;
#6771=DIRECTION ( 'NONE',  ( -3.773278334453079618E-23, 0.9999999999976377785, 2.173523156925979975E-06 ) ) ;
#6772=CARTESIAN_POINT ( 'NONE',  ( -2.938769918389303459, -22.12206158279486345, 11.49999999999999645 ) ) ;
#6774=CARTESIAN_POINT ( 'NONE',  ( -40.62287095715004170, -29.50248789122583659, 2.256150453626215580 ) ) ;
#6775=CARTESIAN_POINT ( 'NONE',  ( -72.58953762381671027, -24.65952944569304250, 1.056160979905694131 ) ) ;
#6777=ORIENTED_EDGE ( 'NONE', *, *, #22783, .T. ) ;
#6780=CARTESIAN_POINT ( 'NONE',  ( -44.62287095715003460, -24.33832256527048088, 0.1851278514138565146 ) ) ;
#6781=CARTESIAN_POINT ( 'NONE',  ( -14.68016216564755894, -15.32010671487267572, 11.49999999999998934 ) ) ;
#6784=CARTESIAN_POINT ( 'NONE',  ( -79.38827465850120291, -25.27791877533765685, 7.124171434988036289 ) ) ;
#6785=CARTESIAN_POINT ( 'NONE',  ( -99.52287095715006160, -24.64898659630529565, 1.056161002820829697 ) ) ;
#6788=CARTESIAN_POINT ( 'NONE',  ( -37.62287095715004881, -23.96177878511307568, 10.65340807706330395 ) ) ;
#6789=CARTESIAN_POINT ( 'NONE',  ( -39.97837580656372580, -25.32724636324322987, 4.398074533285874388 ) ) ;
#6791=CARTESIAN_POINT ( 'NONE',  ( 18.22972481837485859, -6.773019484731225504, 11.49999999999999645 ) ) ;
#6792=DIRECTION ( 'NONE',  ( 0.000000000000000000, 2.173523156925980399E-06, -0.9999999999976378895 ) ) ;
#6793=EDGE_CURVE ( 'NONE', #1776, #89773, #83814, .T. ) ;
#6795=PLANE ( 'NONE',  #68598 ) ;
#6797=EDGE_CURVE ( 'NONE', #12095, #38848, #1523, .T. ) ;
#6798=CARTESIAN_POINT ( 'NONE',  ( -40.62287095715005592, -29.50250243563736774, 8.947779886222148704 ) ) ;
#6802=CARTESIAN_POINT ( 'NONE',  ( -15.21066300689680872, 12.40131300380995860, 11.49999999999998934 ) ) ;
#6803=CARTESIAN_POINT ( 'NONE',  ( -120.2228709571500644, -23.47596703998600631, 11.44779298504227860 ) ) ;
#6805=ORIENTED_EDGE ( 'NONE', *, *, #61204, .T. ) ;
#6807=CARTESIAN_POINT ( 'NONE',  ( 21.48638754631891246, 1.654510534108022179, -1.500000000000002220 ) ) ;
#6809=CARTESIAN_POINT ( 'NONE',  ( -40.62378909974164998, -25.00158670708910336, 2.256160236439222366 ) ) ;
#6811=CARTESIAN_POINT ( 'NONE',  ( -18.27982475084466785, -14.08179083545084964, -1.500000000000002220 ) ) ;
#6813=CARTESIAN_POINT ( 'NONE',  ( -93.50738165881485031, -24.51314013834316796, 0.6176544820404163971 ) ) ;
#6814=CARTESIAN_POINT ( 'NONE',  ( -50.70464068992656337, -25.25249061358302782, 3.767456410489268936 ) ) ;
#6815=CARTESIAN_POINT ( 'NONE',  ( 0.3675393366473880818, 20.13074986235200470, 11.49999999999999645 ) ) ;
#6816=CARTESIAN_POINT ( 'NONE',  ( -121.5883697052726404, -24.66019654487200441, 8.947790411086119278 ) ) ;
#6818=CARTESIAN_POINT ( 'NONE',  ( -111.4457194297752807, -25.29823926093160225, 3.361188652080160377 ) ) ;
#6822=CARTESIAN_POINT ( 'NONE',  ( 2.793900936927258272, 19.68708943014846469, 11.49999999999998934 ) ) ;
#6825=CARTESIAN_POINT ( 'NONE',  ( 2.545096341412688812, 19.61957628810408849, -1.500000000000002220 ) ) ;
#6826=CARTESIAN_POINT ( 'NONE',  ( -42.62870416798130435, -24.51314013834315375, 0.6176544820404090697 ) ) ;
#6827=FACE_OUTER_BOUND ( 'NONE', #92313, .T. ) ;
#6828=FACE_OUTER_BOUND ( 'NONE', #44302, .T. ) ;
#6829=CARTESIAN_POINT ( 'NONE',  ( -0.2510023010970363067, -20.70922355669356563, 11.49999999999999645 ) ) ;
#6830=CARTESIAN_POINT ( 'NONE',  ( -58.52287095715006870, -24.33832256527049154, 0.1851278514138590403 ) ) ;
#6831=EDGE_CURVE ( 'NONE', #47882, #25230, #74180, .T. ) ;
#6832=CARTESIAN_POINT ( 'NONE',  ( -49.59985430115347071, -25.31439339618379947, 5.484775475632647002 ) ) ;
#6833=B_SPLINE_CURVE_WITH_KNOTS ( 'NONE', 3,
 ( #86265, #77639, #71555, #1540 ),
 .UNSPECIFIED., .F., .F.,
 ( 4, 4 ),
 ( 0.000000000000000000, 9.999999999998206125E-05 ),
 .UNSPECIFIED. ) ;
#6834=CARTESIAN_POINT ( 'NONE',  ( 19.36006514395606004, 11.85157241509795512, 11.49999999999999645 ) ) ;
#6836=ORIENTED_EDGE ( 'NONE', *, *, #47177, .F. ) ;
#6837=B_SPLINE_SURFACE_WITH_KNOTS ( 'NONE', 3, 3, ( 
 ( #81451, #25654, #42407, #19535 ),
 ( #87556, #42892, #56125, #87051 ),
 ( #9927, #40882, #18042, #71842 ),
 ( #64248, #49007, #52496, #98647 ),
 ( #21026, #44890, #66244, #67733 ),
 ( #5810, #67232, #5311, #51003 ),
 ( #97661, #60119, #44389, #27663 ) ),
 .UNSPECIFIED., .F., .F., .F.,
 ( 4, 3, 4 ),
 ( 4, 4 ),
 ( 0.0004766839783815690558, 0.1029713700210891647, 0.2054660560637967537 ),
 ( 0.8397076045168327951, 0.8411077686186837488 ),
 .UNSPECIFIED. ) ;
#6840=CARTESIAN_POINT ( 'NONE',  ( -69.90382545228106892, -25.13695321101799252, 7.020456727309716705 ) ) ;
#6841=CARTESIAN_POINT ( 'NONE',  ( -13.64458216870221818, 14.86554040878868044, 11.49999999999998934 ) ) ;
#6842=B_SPLINE_CURVE_WITH_KNOTS ( 'NONE', 3,
 ( #41546, #18686, #49663, #51146, #25812, #73000 ),
 .UNSPECIFIED., .F., .F.,
 ( 4, 2, 4 ),
 ( 1.570755371634013412E-05, 0.001396183895866086886, 0.002776660238015833410 ),
 .UNSPECIFIED. ) ;
#6843=CARTESIAN_POINT ( 'NONE',  ( -63.55376365945738826, -23.96119346886879597, -0.6495511937832106897 ) ) ;
#6844=EDGE_CURVE ( 'NONE', #38183, #84725, #75365, .T. ) ;
#6845=PLANE ( 'NONE',  #26921 ) ;
#6846=ORIENTED_EDGE ( 'NONE', *, *, #42811, .T. ) ;
#6850=CARTESIAN_POINT ( 'NONE',  ( -17.51315278866654879, 14.73147661606379621, 11.49999999999998934 ) ) ;
#6851=CARTESIAN_POINT ( 'NONE',  ( -40.62294849466940860, -25.12194742856580376, 2.840355672353660044 ) ) ;
#6853=CARTESIAN_POINT ( 'NONE',  ( -11.89702471719568244, -18.04982639819725776, -1.500000000000002220 ) ) ;
#6854=CARTESIAN_POINT ( 'NONE',  ( -123.5215661119650292, -23.73766607897670866, -1.055555164236449350 ) ) ;
#6855=FACE_OUTER_BOUND ( 'NONE', #84966, .T. ) ;
#6857=CARTESIAN_POINT ( 'NONE',  ( 10.02768300834196502, -18.34552750054021786, 11.49999999999999645 ) ) ;
#6858=EDGE_LOOP ( 'NONE', ( #53462, #39057, #27222, #49591 ) ) ;
#6861=CARTESIAN_POINT ( 'NONE',  ( -10.13730173486854369, -19.54584281717935568, -1.500000000000002220 ) ) ;
#6862=CARTESIAN_POINT ( 'NONE',  ( -105.5848496801880856, -25.00182538069147142, 7.747789668545044250 ) ) ;
#6863=CARTESIAN_POINT ( 'NONE',  ( -29.00356289826891754, -24.79700109271441022, 6.647731354146906746 ) ) ;
#6864=ORIENTED_EDGE ( 'NONE', *, *, #7552, .T. ) ;
#6866=CARTESIAN_POINT ( 'NONE',  ( -90.64712538269208153, -23.48786465467241058, 11.44779295918254824 ) ) ;
#6868=CARTESIAN_POINT ( 'NONE',  ( -80.52287095715006160, -29.50248789122583659, 2.256150453626215580 ) ) ;
#6869=ORIENTED_EDGE ( 'NONE', *, *, #67803, .T. ) ;
#6870=ORIENTED_EDGE ( 'NONE', *, *, #31195, .F. ) ;
#6871=CARTESIAN_POINT ( 'NONE',  ( -41.52287095715006870, -24.64965694238406613, 8.947790433994205372 ) ) ;
#6872=LINE ( 'NONE', #31709, #93993 ) ;
#6873=CARTESIAN_POINT ( 'NONE',  ( -57.53788008658175102, -24.51314013834315375, 0.6176544820404114011 ) ) ;
#6874=CARTESIAN_POINT ( 'NONE',  ( 12.80116962295325322, 15.99954467330607244, -1.500000000000002220 ) ) ;
#6875=EDGE_LOOP ( 'NONE', ( #40375, #26746, #96574, #81758 ) ) ;
#6877=LINE ( 'NONE', #98726, #40081 ) ;
#6879=CARTESIAN_POINT ( 'NONE',  ( 2.321567282091853812, -22.14299765706108403, 11.49999999999998934 ) ) ;
#6882=CARTESIAN_POINT ( 'NONE',  ( -85.52287095715006160, -29.50250786944525672, 11.44777988621623344 ) ) ;
#6885=CARTESIAN_POINT ( 'NONE',  ( -29.81116385467300489, -24.63645367248981799, 5.042946918296252079 ) ) ;
#6887=CARTESIAN_POINT ( 'NONE',  ( 14.74948264216024008, 14.65492983226340407, -1.500000000000002220 ) ) ;
#6889=PLANE ( 'NONE',  #77904 ) ;
#6890=EDGE_LOOP ( 'NONE', ( #11507, #45357, #2658, #49101 ) ) ;
#6891=AXIS2_PLACEMENT_3D ( 'NONE', #87182, #42526, #48643 ) ;
#6892=DIRECTION ( 'NONE',  ( -3.773278334453079030E-23, 0.9999999999976377785, 2.173523156925979128E-06 ) ) ;
#6893=VERTEX_POINT ( 'NONE', #27008 ) ;
#6894=ORIENTED_EDGE ( 'NONE', *, *, #93198, .F. ) ;
#6896=CARTESIAN_POINT ( 'NONE',  ( -43.62287095715004881, -29.50247984919015209, -1.443849546365060466 ) ) ;
#6897=CARTESIAN_POINT ( 'NONE',  ( -117.5801323110720489, -25.21753527833458364, 3.539999278834443874 ) ) ;
#6899=CARTESIAN_POINT ( 'NONE',  ( -100.4979344782931037, -25.25419553985774712, 7.562057461207404963 ) ) ;
#6900=CARTESIAN_POINT ( 'NONE',  ( -108.9621161194473871, -25.27386152548063691, 3.991943336111062113 ) ) ;
#6901=DIRECTION ( 'NONE',  ( -1.000000000000000000, -3.773278334444166432E-23, -8.201307841325785021E-29 ) ) ;
#6902=CARTESIAN_POINT ( 'NONE',  ( -22.12685673520133989, -0.1325007643398395663, 11.49999999999999645 ) ) ;
#6903=ORIENTED_EDGE ( 'NONE', *, *, #6911, .T. ) ;
#6904=CARTESIAN_POINT ( 'NONE',  ( -91.12544342272609299, -25.36326615310542465, 5.213196219967858092 ) ) ;
#6905=CARTESIAN_POINT ( 'NONE',  ( -17.75566480456612695, 14.03706703302619374, 11.49999999999998934 ) ) ;
#6908=EDGE_LOOP ( 'NONE', ( #27920, #47981, #80057, #3712 ) ) ;
#6909=CARTESIAN_POINT ( 'NONE',  ( -61.64687923781919920, -25.13069339737145214, 2.947789366383932297 ) ) ;
#6911=EDGE_CURVE ( 'NONE', #45335, #84371, #40341, .T. ) ;
#6912=CARTESIAN_POINT ( 'NONE',  ( -13.04681709000290013, -15.30929823114697541, -1.500000000000002220 ) ) ;
#6913=CARTESIAN_POINT ( 'NONE',  ( -88.62287095715004170, -23.48783264082479150, -1.443836473390063935 ) ) ;
#6915=EDGE_CURVE ( 'NONE', #11149, #77509, #66599, .T. ) ;
#6916=CARTESIAN_POINT ( 'NONE',  ( -40.25541618970063240, -25.30507957132854102, 5.538673484309292405 ) ) ;
#6917=B_SPLINE_CURVE_WITH_KNOTS ( 'NONE', 3,
 ( #98842, #23719, #45080, #6508 ),
 .UNSPECIFIED., .F., .F.,
 ( 4, 4 ),
 ( 1.173777234769030585E-05, 0.001966071429883386491 ),
 .UNSPECIFIED. ) ;
#6918=CARTESIAN_POINT ( 'NONE',  ( 21.44611857939883137, 6.294191480875499067, -1.500000000000002220 ) ) ;
#6919=EDGE_LOOP ( 'NONE', ( #23829, #62040, #57181, #18603 ) ) ;
#6921=CARTESIAN_POINT ( 'NONE',  ( -101.5363578631102541, -25.16257311046121714, 6.270899588959630400 ) ) ;
#6922=CARTESIAN_POINT ( 'NONE',  ( -81.85688277028242510, -25.21766921460215016, 6.464279381724344908 ) ) ;
#6923=DIRECTION ( 'NONE',  ( -3.773278334453079030E-23, 0.9999999999976377785, 2.173523156925979128E-06 ) ) ;
#6928=CARTESIAN_POINT ( 'NONE',  ( 14.87128047407919951, 12.67365258641725312, 11.49999999999998934 ) ) ;
#6932=CARTESIAN_POINT ( 'NONE',  ( -16.43003769262999469, -13.82051474754189258, -1.500000000000002220 ) ) ;
#6933=CARTESIAN_POINT ( 'NONE',  ( -25.74893805332498076, -24.57999845255926985, 3.231002331236078717 ) ) ;
#6934=CARTESIAN_POINT ( 'NONE',  ( -107.5228709571500758, -29.50247984919015209, -1.443849546365048253 ) ) ;
#6935=CARTESIAN_POINT ( 'NONE',  ( -47.62287095715004881, -23.47593901973091235, -1.443836447539009749 ) ) ;
#6936=CARTESIAN_POINT ( 'NONE',  ( -14.01358469492184966, -18.07645309290061064, -1.500000000000002220 ) ) ;
#6939=CARTESIAN_POINT ( 'NONE',  ( -108.5228709571500900, -24.34917612407030063, 0.1852690917476662869 ) ) ;
#6940=CARTESIAN_POINT ( 'NONE',  ( 6.088051586893210576, -19.00464151315268424, 11.49999999999999645 ) ) ;
#6941=PLANE ( 'NONE',  #90579 ) ;
#6944=VERTEX_POINT ( 'NONE', #12763 ) ;
#6945=CARTESIAN_POINT ( 'NONE',  ( -27.24283614821936439, -24.59459705238057836, 1.681040237769488854 ) ) ;
#6947=CARTESIAN_POINT ( 'NONE',  ( -96.52287095715010423, -23.48783264082477018, -1.443836473390086139 ) ) ;
#6948=CARTESIAN_POINT ( 'NONE',  ( 16.02445091669267185, 14.69945503153335764, -1.500000000000002220 ) ) ;
#6949=CARTESIAN_POINT ( 'NONE',  ( -56.62287095715008434, -24.35013146730203815, 9.818937971375106599 ) ) ;
#6950=CARTESIAN_POINT ( 'NONE',  ( -18.73025074496528219, 5.678645368852136777, -1.500000000000002220 ) ) ;
#6951=CARTESIAN_POINT ( 'NONE',  ( -61.52287095715006160, -29.50247984919015209, -1.443849546365056913 ) ) ;
#6953=ADVANCED_FACE ( 'NONE', ( #7151 ), #45233, .T. ) ;
#6954=B_SPLINE_CURVE_WITH_KNOTS ( 'NONE', 3,
 ( #69498, #100414, #75587, #7089 ),
 .UNSPECIFIED., .F., .F.,
 ( 4, 4 ),
 ( 0.000000000000000000, 9.999999999998900014E-05 ),
 .UNSPECIFIED. ) ;
#6957=CARTESIAN_POINT ( 'NONE',  ( -116.5228709571500616, -29.50248528299804818, 1.056150453629045360 ) ) ;
#6958=LINE ( 'NONE', #22165, #97762 ) ;
#6959=CARTESIAN_POINT ( 'NONE',  ( -16.48689143942861079, 12.14541645011370541, 11.49999999999999645 ) ) ;
#6961=B_SPLINE_CURVE_WITH_KNOTS ( 'NONE', 3,
 ( #32783, #86068, #71859, #2348 ),
 .UNSPECIFIED., .F., .F.,
 ( 4, 4 ),
 ( 0.000000000000000000, 9.999999999998897304E-05 ),
 .UNSPECIFIED. ) ;
#6962=ADVANCED_FACE ( 'NONE', ( #76156 ), #7675, .T. ) ;
#6963=CARTESIAN_POINT ( 'NONE',  ( -37.52287095715006870, -29.50247984919015209, -1.443849546365060466 ) ) ;
#6972=DIRECTION ( 'NONE',  ( 0.000000000000000000, 2.173523156925980399E-06, -0.9999999999976378895 ) ) ;
#6973=EDGE_CURVE ( 'NONE', #99016, #51651, #52376, .T. ) ;
#6974=CARTESIAN_POINT ( 'NONE',  ( 10.19088217375349892, 20.72639945755932800, 11.49999999999999645 ) ) ;
#6975=CARTESIAN_POINT ( 'NONE',  ( 9.312063170398973355, -20.82641193498425025, 11.49999999999998934 ) ) ;
#6976=CARTESIAN_POINT ( 'NONE',  ( -109.6228709571500559, -24.64965695001469115, 8.947790433994176951 ) ) ;
#6977=B_SPLINE_SURFACE_WITH_KNOTS ( 'NONE', 3, 1, ( 
 ( #17061, #55647 ),
 ( #30793, #15061 ),
 ( #46030, #77942 ),
 ( #46520, #16550 ),
 ( #94180, #77448 ),
 ( #32291, #69860 ),
 ( #61261, #70357 ),
 ( #85073, #7445 ),
 ( #23157, #48028 ),
 ( #47527, #62765 ),
 ( #54150, #38401 ),
 ( #78953, #78450 ),
 ( #63261, #23666 ),
 ( #31286, #61760 ),
 ( #62254, #38902 ) ),
 .UNSPECIFIED., .F., .F., .F.,
 ( 4, 1, 1, 1, 1, 1, 1, 1, 1, 1, 1, 1, 4 ),
 ( 2, 2 ),
 ( 0.000000000000000000, 0.1108026438013187259, 0.2128292023477701411, 0.3061013098231112339, 0.3906473211160097492, 0.4669244693608501917, 0.5344810392840317892, 0.5935869409656733264, 0.6445570045087155586, 0.7362004526293723927, 0.8250240256188635657, 0.9119855848297575562, 1.000000000000000000 ),
 ( 0.000000000000000000, 1.000000000000000000 ),
 .UNSPECIFIED. ) ;
#6980=DIRECTION ( 'NONE',  ( 3.773278334444167608E-23, -1.000000000000000000, 0.000000000000000000 ) ) ;
#6982=EDGE_CURVE ( 'NONE', #38959, #18132, #82781, .T. ) ;
#6983=CARTESIAN_POINT ( 'NONE',  ( -8.322136096487577461, -20.27582920440508829, -1.500000000000002220 ) ) ;
#6985=CARTESIAN_POINT ( 'NONE',  ( -109.6228709571500417, -24.65952944569305316, 1.056160979905704345 ) ) ;
#6987=CARTESIAN_POINT ( 'NONE',  ( -78.63771738212270179, -23.96119346886880308, -0.6495511937832113558 ) ) ;
#6988=CARTESIAN_POINT ( 'NONE',  ( -117.6228709571500559, -24.64898659630368627, 1.056161002820833028 ) ) ;
#6990=CARTESIAN_POINT ( 'NONE',  ( 18.81987132735423174, -8.002443037797982939, -1.500000000000002220 ) ) ;
#6992=ORIENTED_EDGE ( 'NONE', *, *, #2471, .T. ) ;
#6995=ORIENTED_EDGE ( 'NONE', *, *, #37008, .T. ) ;
#6996=CARTESIAN_POINT ( 'NONE',  ( 1.912052097559287844, -22.98750448113701239, 11.49999999999998934 ) ) ;
#6997=CARTESIAN_POINT ( 'NONE',  ( -61.50413361299347770, -24.15543982623907127, -0.2315651400026656481 ) ) ;
#6998=CARTESIAN_POINT ( 'NONE',  ( -6.993686169601437186, 18.98418669460116348, -1.500000000000002220 ) ) ;
#7000=ORIENTED_EDGE ( 'NONE', *, *, #71475, .T. ) ;
#7001=CARTESIAN_POINT ( 'NONE',  ( -54.52287095715006870, -24.64965694238575011, 8.947790433994203596 ) ) ;
#7004=CARTESIAN_POINT ( 'NONE',  ( -70.50072534953635284, -24.40034930558990922, 0.3402023900116040167 ) ) ;
#7005=CARTESIAN_POINT ( 'NONE',  ( 2.695732861974529104, -21.29187259674557708, 11.49999999999999645 ) ) ;
#7007=CARTESIAN_POINT ( 'NONE',  ( -113.6228709571500559, -23.94994826722516379, -0.6494450866351674234 ) ) ;
#7008=CARTESIAN_POINT ( 'NONE',  ( -110.6228709571500559, -23.47593901973091235, -1.443836447538999312 ) ) ;
#7011=CARTESIAN_POINT ( 'NONE',  ( 16.32338804990218151, -12.73490195939593406, 11.49999999999998934 ) ) ;
#7012=ORIENTED_EDGE ( 'NONE', *, *, #33342, .T. ) ;
#7016=VERTEX_POINT ( 'NONE', #59967 ) ;
#7018=B_SPLINE_CURVE_WITH_KNOTS ( 'NONE', 3,
 ( #16194, #77584, #7087, #30423, #38038, #68989 ),
 .UNSPECIFIED., .F., .F.,
 ( 4, 2, 4 ),
 ( 0.000000000000000000, 0.001380901958385390062, 0.002761803916770780125 ),
 .UNSPECIFIED. ) ;
#7019=CARTESIAN_POINT ( 'NONE',  ( -102.5228709571500758, -23.47596703998600631, 11.44779298504228215 ) ) ;
#7020=CARTESIAN_POINT ( 'NONE',  ( 7.969717912702302343, -20.46423023992739942, 11.49999999999999645 ) ) ;
#7021=CARTESIAN_POINT ( 'NONE',  ( -89.55819837874346945, -23.73791477778911840, 11.05961554403170410 ) ) ;
#7022=CARTESIAN_POINT ( 'NONE',  ( 21.78986343443989071, 5.811249688775594002, 11.49999999999998934 ) ) ;
#7023=CARTESIAN_POINT ( 'NONE',  ( -7.180602670292889123, -19.69607742855361465, -1.500000000000002220 ) ) ;
#7024=CARTESIAN_POINT ( 'NONE',  ( -109.0053741199720747, -25.30783060902023252, 4.561566455935911257 ) ) ;
#7025=VECTOR ( 'NONE', #57656, 1000.000000000000114 ) ;
#7029=ORIENTED_EDGE ( 'NONE', *, *, #66075, .F. ) ;
#7030=CARTESIAN_POINT ( 'NONE',  ( -36.62287095715006302, -24.51283580621364067, 0.6167428607019720399 ) ) ;
#7031=CARTESIAN_POINT ( 'NONE',  ( 13.13055478438326773, -17.03443908202477886, -1.500000000000002220 ) ) ;
#7033=CARTESIAN_POINT ( 'NONE',  ( -90.62287095715001328, -24.14406661707770851, 10.28769366152061870 ) ) ;
#7035=CARTESIAN_POINT ( 'NONE',  ( -16.97324839047195866, 12.58421825509937442, 11.49999999999998934 ) ) ;
#7037=ADVANCED_FACE ( 'NONE', ( #5658 ), #98494, .T. ) ;
#7038=CARTESIAN_POINT ( 'NONE',  ( -64.62365164054095601, -24.65952944569304250, 1.056160979905695685 ) ) ;
#7039=CARTESIAN_POINT ( 'NONE',  ( -50.33479198164290125, -25.30263672226421079, 4.734682818538147764 ) ) ;
#7041=CARTESIAN_POINT ( 'NONE',  ( -123.5895376238167387, -23.48783264082478794, -1.443836473390058606 ) ) ;
#7042=CARTESIAN_POINT ( 'NONE',  ( 12.08182546098005972, -18.57710416600862402, -1.500000000000002220 ) ) ;
#7044=FACE_OUTER_BOUND ( 'NONE', #16373, .T. ) ;
#7049=DIRECTION ( 'NONE',  ( 0.000000000000000000, -0.9999999999976377785, -2.173523156925979975E-06 ) ) ;
#7050=ADVANCED_FACE ( 'NONE', ( #47733 ), #54847, .T. ) ;
#7052=CARTESIAN_POINT ( 'NONE',  ( 1.255614643274026276, -19.41590359075080841, 11.49999999999998934 ) ) ;
#7053=CARTESIAN_POINT ( 'NONE',  ( 2.027878592902508270, 21.29203748114955985, -1.500000000000002220 ) ) ;
#7054=CARTESIAN_POINT ( 'NONE',  ( -62.49105905257930260, -24.65952944569303895, 1.056160979905693686 ) ) ;
#7057=CARTESIAN_POINT ( 'NONE',  ( -109.5228709571500616, -29.50247984919015209, -1.443849546365048253 ) ) ;
#7058=CARTESIAN_POINT ( 'NONE',  ( 1.118074629359579797, -22.68859683979520980, -1.500000000000002220 ) ) ;
#7059=B_SPLINE_SURFACE_WITH_KNOTS ( 'NONE', 3, 3, ( 
 ( #24702, #72401, #31831, #86110 ),
 ( #17602, #88123, #9986, #25205 ),
 ( #33825, #56183, #2895, #64812 ),
 ( #49566, #16587, #26216, #18590 ),
 ( #47564, #55682, #80497, #78485 ),
 ( #8984, #70899, #86610, #1390 ),
 ( #17097, #36327, #72901, #5374 ) ),
 .UNSPECIFIED., .F., .F., .F.,
 ( 4, 3, 4 ),
 ( 4, 4 ),
 ( 0.7945040050992242531, 0.8970133687736503436, 0.9995227324480764342 ),
 ( 0.8197022949557353222, 0.8210934484848215753 ),
 .UNSPECIFIED. ) ;
#7060=EDGE_CURVE ( 'NONE', #1645, #44267, #48801, .T. ) ;
#7062=CARTESIAN_POINT ( 'NONE',  ( -87.52287095715006160, -24.66019654487200086, 8.947790411086115725 ) ) ;
#7064=CARTESIAN_POINT ( 'NONE',  ( 2.545096341412688812, 19.61957628810408849, 11.49999999999999645 ) ) ;
#7065=DIRECTION ( 'NONE',  ( 3.773278334444166432E-23, -1.000000000000000000, 0.000000000000000000 ) ) ;
#7067=CARTESIAN_POINT ( 'NONE',  ( -59.52287095715004028, -23.94994826722564696, -0.6494450866342711404 ) ) ;
#7069=CARTESIAN_POINT ( 'NONE',  ( -61.64687923781919210, -25.21083105912962452, 3.409327675794633361 ) ) ;
#7070=CARTESIAN_POINT ( 'NONE',  ( 14.58690015069645263, 15.99052346098381250, 11.49999999999998934 ) ) ;
#7072=CARTESIAN_POINT ( 'NONE',  ( -16.37229413335033001, -10.43475415037859655, -1.500000000000002220 ) ) ;
#7073=CARTESIAN_POINT ( 'NONE',  ( -129.6228709571500133, -23.73934037231757799, 11.05740245334328087 ) ) ;
#7074=CARTESIAN_POINT ( 'NONE',  ( -40.58953762381671737, -24.99156044556120193, 7.747789690856344613 ) ) ;
#7075=CARTESIAN_POINT ( 'NONE',  ( 18.95923836289803788, 5.684714004613049987, 11.49999999999998934 ) ) ;
#7076=B_SPLINE_CURVE_WITH_KNOTS ( 'NONE', 3,
 ( #26179, #73856, #11949, #89082 ),
 .UNSPECIFIED., .F., .F.,
 ( 4, 4 ),
 ( 2.613633516198037533E-05, 0.004366793516964704441 ),
 .UNSPECIFIED. ) ;
#7077=VERTEX_POINT ( 'NONE', #15264 ) ;
#7078=AXIS2_PLACEMENT_3D ( 'NONE', #47787, #9206, #40168 ) ;
#7079=CARTESIAN_POINT ( 'NONE',  ( -12.25758032491116367, 16.21837406056298292, 11.49999999999999645 ) ) ;
#7080=FACE_OUTER_BOUND ( 'NONE', #74906, .T. ) ;
#7081=CARTESIAN_POINT ( 'NONE',  ( -46.52287095715004028, -24.66019654487199375, 8.947790411086122830 ) ) ;
#7082=ORIENTED_EDGE ( 'NONE', *, *, #57484, .F. ) ;
#7083=CARTESIAN_POINT ( 'NONE',  ( -30.60515864328932878, -24.57438384523503672, 0.5319095616429414530 ) ) ;
#7084=CARTESIAN_POINT ( 'NONE',  ( -116.4728709594060092, -25.21147767946276019, 8.000950762517433645 ) ) ;
#7085=CARTESIAN_POINT ( 'NONE',  ( -48.87464133331025806, -25.31602070427312867, 6.106124868286230800 ) ) ;
#7086=CARTESIAN_POINT ( 'NONE',  ( -40.48178299873823960, -24.63419186844611630, 9.035850630976923981 ) ) ;
#7087=CARTESIAN_POINT ( 'NONE',  ( -127.6228709571500559, -23.95044443724992078, 10.65354141964649415 ) ) ;
#7088=CARTESIAN_POINT ( 'NONE',  ( -18.95788008782500356, -6.583919088883305015, 11.49999999999998934 ) ) ;
#7089=CARTESIAN_POINT ( 'NONE',  ( -95.52287095715006160, -24.99132157543166954, 2.256160258750667502 ) ) ;
#7090=EDGE_LOOP ( 'NONE', ( #23115, #21331, #372, #53139 ) ) ;
#7093=B_SPLINE_CURVE_WITH_KNOTS ( 'NONE', 3,
 ( #97043, #51877, #83304, #89930, #8067, #36148, #50881, #5687 ),
 .UNSPECIFIED., .F., .F.,
 ( 4, 2, 2, 4 ),
 ( 0.000000000000000000, 0.002001098010032677579, 0.003001647015049018104, 0.004002196020065359496 ),
 .UNSPECIFIED. ) ;
#7094=CARTESIAN_POINT ( 'NONE',  ( -22.64140897529919272, -3.284158816904186651, 11.49999999999999645 ) ) ;
#7095=CARTESIAN_POINT ( 'NONE',  ( -5.793434319722853054, -21.96748078227757617, 11.49999999999998934 ) ) ;
#7096=CARTESIAN_POINT ( 'NONE',  ( -49.94769165354211538, -25.31297195507654507, 4.634772910520919886 ) ) ;
#7097=CARTESIAN_POINT ( 'NONE',  ( -50.62287095715005592, -23.47596703998600631, 11.44779298504227505 ) ) ;
#7098=CARTESIAN_POINT ( 'NONE',  ( -38.66565014046062032, -23.48786465467240347, 11.44779295918255002 ) ) ;
#7100=EDGE_CURVE ( 'NONE', #61887, #10751, #35498, .T. ) ;
#7101=CARTESIAN_POINT ( 'NONE',  ( -128.5556214221262223, -24.35071581493544102, 9.817618358456019934 ) ) ;
#7105=CARTESIAN_POINT ( 'NONE',  ( 19.36038471569032993, -6.267470172042458820, 11.49999999999998934 ) ) ;
#7108=CARTESIAN_POINT ( 'NONE',  ( -21.75629724252761577, 7.406401271465676395, 11.49999999999998934 ) ) ;
#7109=CARTESIAN_POINT ( 'NONE',  ( -32.47729921221014138, -24.65952944569304606, 1.056160979905696351 ) ) ;
#7112=CARTESIAN_POINT ( 'NONE',  ( -94.58953762381672448, -23.48783264082478794, -1.443836473390063491 ) ) ;
#7114=CARTESIAN_POINT ( 'NONE',  ( -19.44786352930952233, -8.617208915446557427, 11.49999999999999645 ) ) ;
#7116=ORIENTED_EDGE ( 'NONE', *, *, #20946, .F. ) ;
#7117=CARTESIAN_POINT ( 'NONE',  ( 21.18294168759468832, 6.642818831845659133, 11.49999999999998934 ) ) ;
#7118=CARTESIAN_POINT ( 'NONE',  ( -18.09956831669839872, 9.893135806712603397, 11.49999999999998934 ) ) ;
#7119=ORIENTED_EDGE ( 'NONE', *, *, #78191, .F. ) ;
#7120=ORIENTED_EDGE ( 'NONE', *, *, #31626, .T. ) ;
#7121=CARTESIAN_POINT ( 'NONE',  ( -109.1250679552890830, -25.27682725309280087, 4.858945224259093365 ) ) ;
#7124=CARTESIAN_POINT ( 'NONE',  ( -49.74249510286006171, -25.16055632220097138, 6.938864448453002431 ) ) ;
#7125=ORIENTED_EDGE ( 'NONE', *, *, #92475, .F. ) ;
#7126=CARTESIAN_POINT ( 'NONE',  ( -39.52287095715006160, -24.50321055353803956, 9.387540953477529371 ) ) ;
#7127=CARTESIAN_POINT ( 'NONE',  ( -35.62287095715005592, -23.48786465467240347, 11.44779295918255180 ) ) ;
#7128=CARTESIAN_POINT ( 'NONE',  ( 18.76864855846692492, -9.085702381504452418, -1.500000000000002220 ) ) ;
#7129=CARTESIAN_POINT ( 'NONE',  ( -19.23829340896090656, 10.21096329589227025, 11.49999999999999645 ) ) ;
#7131=CARTESIAN_POINT ( 'NONE',  ( -100.5372941577377617, -25.18545306133426465, 3.297626459260741161 ) ) ;
#7132=CARTESIAN_POINT ( 'NONE',  ( -78.52212882731420507, -23.48786465467241058, 11.44779295918254469 ) ) ;
#7133=CARTESIAN_POINT ( 'NONE',  ( 21.16529133594374557, -7.503415950508986576, -1.500000000000002220 ) ) ;
#7134=CARTESIAN_POINT ( 'NONE',  ( -43.62287095715004881, -24.66019654487199020, 8.947790411086135265 ) ) ;
#7138=CARTESIAN_POINT ( 'NONE',  ( -101.8161100070499572, -25.24282061761980955, 6.236250683194342059 ) ) ;
#7139=B_SPLINE_CURVE_WITH_KNOTS ( 'NONE', 3,
 ( #61006, #75704, #98542, #30031, #60015, #91940, #84321, #91430 ),
 .UNSPECIFIED., .F., .F.,
 ( 4, 2, 2, 4 ),
 ( -0.001224554619866340642, -0.0002241820295893614135, 0.0007761905606876178150, 0.002776935741241576272 ),
 .UNSPECIFIED. ) ;
#7140=VERTEX_POINT ( 'NONE', #46730 ) ;
#7141=VERTEX_POINT ( 'NONE', #8665 ) ;
#7142=ORIENTED_EDGE ( 'NONE', *, *, #35331, .T. ) ;
#7143=CARTESIAN_POINT ( 'NONE',  ( -21.34312709018487553, 1.176582458498846462, -1.500000000000002220 ) ) ;
#7144=ORIENTED_EDGE ( 'NONE', *, *, #77814, .T. ) ;
#7145=CARTESIAN_POINT ( 'NONE',  ( -19.96636262075925927, 6.592627302904066511, -1.500000000000002220 ) ) ;
#7146=CARTESIAN_POINT ( 'NONE',  ( -30.58285789377789499, -25.15082570009304064, 2.712646531854225440 ) ) ;
#7147=ADVANCED_FACE ( 'NONE', ( #8163 ), #62967, .F. ) ;
#7148=CARTESIAN_POINT ( 'NONE',  ( -99.91491574289003097, -25.20057459230137198, 3.406812263743608682 ) ) ;
#7150=CARTESIAN_POINT ( 'NONE',  ( 14.26656746985186608, 16.74056184347216458, -1.500000000000002220 ) ) ;
#7151=FACE_OUTER_BOUND ( 'NONE', #87779, .T. ) ;
#7152=ORIENTED_EDGE ( 'NONE', *, *, #54736, .T. ) ;
#7153=PLANE ( 'NONE',  #56516 ) ;
#7154=EDGE_CURVE ( 'NONE', #2401, #100041, #7623, .T. ) ;
#7155=CARTESIAN_POINT ( 'NONE',  ( -41.62287095715006302, -24.64965695001467694, 8.947790433994187609 ) ) ;
#7156=ADVANCED_FACE ( 'NONE', ( #71072 ), #55855, .F. ) ;
#7157=CARTESIAN_POINT ( 'NONE',  ( -84.52214524269466267, -23.48786465467241769, 11.44779295918254647 ) ) ;
#7158=EDGE_CURVE ( 'NONE', #77786, #13179, #30622, .T. ) ;
#7160=CARTESIAN_POINT ( 'NONE',  ( -30.60887394897559943, -24.57243507446463937, 9.174899246800711339 ) ) ;
#7161=CARTESIAN_POINT ( 'NONE',  ( 6.557060941508195739, 20.25493142521265355, -1.500000000000002220 ) ) ;
#7162=LINE ( 'NONE', #47744, #57998 ) ;
#7163=EDGE_CURVE ( 'NONE', #63553, #32600, #2791, .T. ) ;
#7164=CARTESIAN_POINT ( 'NONE',  ( -107.6280293522714260, -24.15620529776628800, 10.23563542870659759 ) ) ;
#7166=CARTESIAN_POINT ( 'NONE',  ( -33.64272878514460530, -24.15543982623906771, -0.2315651400026580431 ) ) ;
#7167=CARTESIAN_POINT ( 'NONE',  ( 8.356338879324495039, -20.90460381316865934, -1.500000000000002220 ) ) ;
#7170=CARTESIAN_POINT ( 'NONE',  ( -76.62287095715007013, -23.48786465467241058, 11.44779295918254469 ) ) ;
#7171=CARTESIAN_POINT ( 'NONE',  ( -15.04504930077994196, -12.58455232801425794, 11.49999999999999645 ) ) ;
#7172=CARTESIAN_POINT ( 'NONE',  ( -55.52287095715006870, -25.00182538069145011, 7.747789668545106423 ) ) ;
#7176=CARTESIAN_POINT ( 'NONE',  ( -88.50535495414969489, -24.51419770103157703, 9.386484678747176957 ) ) ;
#7177=CARTESIAN_POINT ( 'NONE',  ( -126.8950052880273063, -25.34772655306150924, 6.200157639293698786 ) ) ;
#7178=CARTESIAN_POINT ( 'NONE',  ( -100.3128489789178559, -25.31439539913989378, 5.229225532754338879 ) ) ;
#7179=CARTESIAN_POINT ( 'NONE',  ( -6.756748142665309764, -18.51622224137248907, -1.500000000000002220 ) ) ;
#7182=CARTESIAN_POINT ( 'NONE',  ( -66.62287095715005592, -29.50248528299804818, 1.056150453629036701 ) ) ;
#7186=DIRECTION ( 'NONE',  ( 0.000000000000000000, -2.173523156925980399E-06, 0.9999999999976378895 ) ) ;
#7190=CARTESIAN_POINT ( 'NONE',  ( -86.62287095715004170, -29.50250243563736774, 8.947779886222139822 ) ) ;
#7193=CARTESIAN_POINT ( 'NONE',  ( -14.92271332039470444, 13.28099397388983327, -1.500000000000002220 ) ) ;
#7195=AXIS2_PLACEMENT_3D ( 'NONE', #94229, #31335, #55696 ) ;
#7196=CARTESIAN_POINT ( 'NONE',  ( -100.3793702452611285, -25.10935038052450352, 2.834178115470032289 ) ) ;
#7197=CARTESIAN_POINT ( 'NONE',  ( -51.57235953973243880, -25.30441124943957476, 4.474666492193762224 ) ) ;
#7199=ADVANCED_FACE ( 'NONE', ( #54828 ), #40600, .T. ) ;
#7200=CARTESIAN_POINT ( 'NONE',  ( -119.5930743455675582, -23.48783264082477018, -1.443836473390087916 ) ) ;
#7201=CARTESIAN_POINT ( 'NONE',  ( -80.54147481932388075, -24.73531770709095312, 8.716586749053508498 ) ) ;
#7203=CARTESIAN_POINT ( 'NONE',  ( -108.5228709571500758, -23.72747288104470442, -1.053458166803225682 ) ) ;
#7204=CARTESIAN_POINT ( 'NONE',  ( -28.41293738586069040, -24.60093919842945098, 1.764153402501565715 ) ) ;
#7207=EDGE_CURVE ( 'NONE', #66840, #16463, #31697, .T. ) ;
#7210=CARTESIAN_POINT ( 'NONE',  ( -2.356373108420451334, 20.14613781377289214, 11.49999999999998934 ) ) ;
#7211=CARTESIAN_POINT ( 'NONE',  ( -85.62287095715004170, -24.99132157543083821, 2.256160258750667502 ) ) ;
#7212=ADVANCED_FACE ( 'NONE', ( #9134 ), #54328, .F. ) ;
#7214=DIRECTION ( 'NONE',  ( 1.000000000000000000, 3.773278334444167608E-23, 8.201307833595939069E-29 ) ) ;
#7215=VERTEX_POINT ( 'NONE', #39082 ) ;
#7216=FACE_OUTER_BOUND ( 'NONE', #34924, .T. ) ;
#7217=CARTESIAN_POINT ( 'NONE',  ( -20.11654390397962544, -0.4351469013266864860, -1.500000000000002220 ) ) ;
#7218=CARTESIAN_POINT ( 'NONE',  ( 7.532573551308565207, 19.69859070278346991, 11.49999999999999645 ) ) ;
#7220=CARTESIAN_POINT ( 'NONE',  ( -32.52287095715006160, -24.65952944569304606, 1.056160979905690134 ) ) ;
#7221=CARTESIAN_POINT ( 'NONE',  ( 7.643743511751816655, -20.74876368896106271, -1.500000000000002220 ) ) ;
#7223=CARTESIAN_POINT ( 'NONE',  ( 19.85418835109896563, -5.301297255791479479, -1.500000000000002220 ) ) ;
#7224=CARTESIAN_POINT ( 'NONE',  ( -35.52287095715006870, -24.99132157543083821, 2.256160258750667502 ) ) ;
#7225=CARTESIAN_POINT ( 'NONE',  ( -126.6228709571500559, -24.64898659630529565, 1.056161002820834804 ) ) ;
#7228=ORIENTED_EDGE ( 'NONE', *, *, #84407, .F. ) ;
#7230=B_SPLINE_SURFACE_WITH_KNOTS ( 'NONE', 3, 3, ( 
 ( #99870, #54735, #54236, #53734 ),
 ( #69940, #84160, #22750, #428 ),
 ( #30377, #78034, #23759, #22250 ),
 ( #15152, #84664, #61349, #93270 ),
 ( #7543, #91768, #61847, #68449 ),
 ( #38990, #77541, #85669, #46620 ),
 ( #45616, #37497, #100365, #60850 ) ),
 .UNSPECIFIED., .F., .F., .F.,
 ( 4, 3, 4 ),
 ( 4, 4 ),
 ( 0.0004766839783818845044, 0.1029713700210894839, 0.2054660560637970868 ),
 ( 0.5896439926061133319, 0.5909287778169047822 ),
 .UNSPECIFIED. ) ;
#7231=DIRECTION ( 'NONE',  ( 1.000000000000000000, 3.773278334444167608E-23, 8.201307833595939069E-29 ) ) ;
#7232=VERTEX_POINT ( 'NONE', #524 ) ;
#7233=ORIENTED_EDGE ( 'NONE', *, *, #37404, .F. ) ;
#7234=ORIENTED_EDGE ( 'NONE', *, *, #86589, .F. ) ;
#7235=CARTESIAN_POINT ( 'NONE',  ( -118.6228709571500559, -24.33832256526968862, 0.1851278514119937824 ) ) ;
#7238=CARTESIAN_POINT ( 'NONE',  ( -19.97286373971314433, -5.326668811655218327, -1.500000000000002220 ) ) ;
#7239=CARTESIAN_POINT ( 'NONE',  ( -7.206546067468990735, 20.34698395366585189, 11.49999999999999645 ) ) ;
#7240=ORIENTED_EDGE ( 'NONE', *, *, #46132, .T. ) ;
#7241=CARTESIAN_POINT ( 'NONE',  ( -81.55620429048337883, -24.66019654487199730, 8.947790411086124607 ) ) ;
#7243=CARTESIAN_POINT ( 'NONE',  ( -1.374798071107336206, -22.32369649477951512, 11.49999999999998934 ) ) ;
#7244=CARTESIAN_POINT ( 'NONE',  ( -80.26303174456680267, -25.27875086665990878, 7.082509052535141514 ) ) ;
#7245=CARTESIAN_POINT ( 'NONE',  ( -104.5228709571500758, -24.64898659630529565, 1.056161002820829697 ) ) ;
#7246=ORIENTED_EDGE ( 'NONE', *, *, #6473, .T. ) ;
#7247=CARTESIAN_POINT ( 'NONE',  ( -116.5120762170639637, -25.40067276019392395, 5.394074047000503747 ) ) ;
#7250=CARTESIAN_POINT ( 'NONE',  ( -20.37482282770194075, 4.769447832466558346, -1.500000000000002220 ) ) ;
#7253=CARTESIAN_POINT ( 'NONE',  ( -86.54257510269528098, -24.65952944569304961, 1.056160979905701680 ) ) ;
#7254=VERTEX_POINT ( 'NONE', #55329 ) ;
#7256=CARTESIAN_POINT ( 'NONE',  ( -109.5495832072082720, -24.66019654487200441, 8.947790411086113949 ) ) ;
#7257=CARTESIAN_POINT ( 'NONE',  ( -12.03079493616482765, -17.41531974249929249, -1.500000000000002220 ) ) ;
#7259=CARTESIAN_POINT ( 'NONE',  ( -117.6281488526506678, -23.73766607897670511, -1.055555164236445798 ) ) ;
#7260=CARTESIAN_POINT ( 'NONE',  ( -99.37409858214790859, -25.26221189400888889, 6.508816812834683496 ) ) ;
#7261=CARTESIAN_POINT ( 'NONE',  ( -19.23829340896090656, 10.21096329589227025, -1.500000000000002220 ) ) ;
#7265=CARTESIAN_POINT ( 'NONE',  ( 18.38516380405726736, -11.72527425286322611, -1.500000000000002220 ) ) ;
#7266=CARTESIAN_POINT ( 'NONE',  ( -71.53293015653792963, -25.24674183039172704, 5.453599235397658340 ) ) ;
#7267=ADVANCED_FACE ( 'NONE', ( #31475 ), #61975, .T. ) ;
#7268=ORIENTED_EDGE ( 'NONE', *, *, #70406, .T. ) ;
#7270=CARTESIAN_POINT ( 'NONE',  ( -117.5228709571500474, -23.94994826722565762, -0.6494450866342728057 ) ) ;
#7274=VERTEX_POINT ( 'NONE', #56339 ) ;
#7275=B_SPLINE_CURVE_WITH_KNOTS ( 'NONE', 3,
 ( #74816, #29146, #13414, #98146 ),
 .UNSPECIFIED., .F., .F.,
 ( 4, 4 ),
 ( 1.387778780781445676E-17, 0.0001000000000000028779 ),
 .UNSPECIFIED. ) ;
#7276=ORIENTED_EDGE ( 'NONE', *, *, #45884, .F. ) ;
#7277=ADVANCED_FACE ( 'NONE', ( #64962 ), #19243, .F. ) ;
#7278=CARTESIAN_POINT ( 'NONE',  ( -124.5228709571500190, -24.66019654487200441, 8.947790411086112172 ) ) ;
#7279=CARTESIAN_POINT ( 'NONE',  ( 20.46717832272283033, -5.532298862796615424, 11.49999999999998934 ) ) ;
#7280=CARTESIAN_POINT ( 'NONE',  ( -94.59134195305344406, -24.15543982623907482, -0.2315651400026595141 ) ) ;
#7282=CARTESIAN_POINT ( 'NONE',  ( -30.64427850938830389, -23.56000036390796737, -1.497999999999532816 ) ) ;
#7284=DIRECTION ( 'NONE',  ( -3.773278334453079618E-23, 0.9999999999976377785, 2.173523156925979975E-06 ) ) ;
#7285=CARTESIAN_POINT ( 'NONE',  ( -18.22047185089115828, 6.579378235550767506, 11.49999999999998934 ) ) ;
#7288=CARTESIAN_POINT ( 'NONE',  ( -17.22176335520693158, -9.073154711715998744, 11.49999999999999645 ) ) ;
#7289=CARTESIAN_POINT ( 'NONE',  ( -42.52287095715005449, -23.47596703998600631, 11.44779298504229281 ) ) ;
#7290=CARTESIAN_POINT ( 'NONE',  ( -49.62287095715004170, -23.47596703998600631, 11.44779298504227505 ) ) ;
#7292=ORIENTED_EDGE ( 'NONE', *, *, #24680, .F. ) ;
#7294=CARTESIAN_POINT ( 'NONE',  ( -70.27422298781921484, -25.30465073045868252, 4.851635164186505200 ) ) ;
#7295=DIRECTION ( 'NONE',  ( -3.773278334444167608E-23, 1.000000000000000000, 0.000000000000000000 ) ) ;
#7296=CARTESIAN_POINT ( 'NONE',  ( -93.50972247225219292, -24.35071581493543746, 9.817618358456018157 ) ) ;
#7297=CARTESIAN_POINT ( 'NONE',  ( -19.61951575358169819, -0.1233725505697131491, 11.49999999999998934 ) ) ;
#7298=CARTESIAN_POINT ( 'NONE',  ( -41.08147698621603894, -25.27806096597225505, 4.883364703189866596 ) ) ;
#7299=ORIENTED_EDGE ( 'NONE', *, *, #11842, .T. ) ;
#7301=CARTESIAN_POINT ( 'NONE',  ( -15.49073194614445015, 15.02706685249526686, 11.49999999999998934 ) ) ;
#7302=PLANE ( 'NONE',  #60958 ) ;
#7303=CARTESIAN_POINT ( 'NONE',  ( -40.46892904929547541, -25.00158670708910336, 2.256160236439222366 ) ) ;
#7304=CARTESIAN_POINT ( 'NONE',  ( -121.5895376238167245, -24.64898659630368627, 1.056161002820393602 ) ) ;
#7305=CARTESIAN_POINT ( 'NONE',  ( -4.971178678486217528, -22.47594730032828281, -1.500000000000002220 ) ) ;
#7307=DIRECTION ( 'NONE',  ( -3.773278334453079030E-23, 0.9999999999976377785, 2.173523156925979128E-06 ) ) ;
#7308=CARTESIAN_POINT ( 'NONE',  ( -89.62287095715004170, -29.50250243563736774, 8.947779886222139822 ) ) ;
#7309=CARTESIAN_POINT ( 'NONE',  ( -4.116507902937485142, 19.75820112358731251, 11.49999999999999645 ) ) ;
#7310=CARTESIAN_POINT ( 'NONE',  ( -121.5222464708741938, -23.48786465467241769, 11.44779295918253759 ) ) ;
#7313=FACE_OUTER_BOUND ( 'NONE', #49930, .T. ) ;
#7314=CARTESIAN_POINT ( 'NONE',  ( -111.1810695982967161, -25.18425674466588760, 3.716321248519699694 ) ) ;
#7315=CARTESIAN_POINT ( 'NONE',  ( 9.006517291608927778, -17.75031788249398446, 11.49999999999998934 ) ) ;
#7317=CARTESIAN_POINT ( 'NONE',  ( -13.31955177964949755, -14.60123061082138385, -1.500000000000002220 ) ) ;
#7318=CARTESIAN_POINT ( 'NONE',  ( -81.52287095715010423, -23.47593901973090524, -1.443836447538996648 ) ) ;
#7320=CARTESIAN_POINT ( 'NONE',  ( -39.32379795506943054, -25.29116634425743726, 3.365606283317699621 ) ) ;
#7322=CARTESIAN_POINT ( 'NONE',  ( -17.23291202157775359, 11.51834372740795231, 11.49999999999999645 ) ) ;
#7323=CARTESIAN_POINT ( 'NONE',  ( -56.62287095715005592, -23.47593901973091235, -1.443836447539007972 ) ) ;
#7325=EDGE_CURVE ( 'NONE', #77908, #68025, #81305, .T. ) ;
#7326=CARTESIAN_POINT ( 'NONE',  ( -106.5222054704709649, -23.48783264082477373, -1.443836473390085695 ) ) ;
#7327=CARTESIAN_POINT ( 'NONE',  ( -22.17926634000774655, 4.976981427743210951, 11.49999999999999645 ) ) ;
#7329=VERTEX_POINT ( 'NONE', #26367 ) ;
#7332=CARTESIAN_POINT ( 'NONE',  ( -19.70923665959843873, 4.302044407003456250, -1.500000000000002220 ) ) ;
#7333=DIRECTION ( 'NONE',  ( 0.000000000000000000, 0.9999999999976377785, 2.173523156925979975E-06 ) ) ;
#7335=CARTESIAN_POINT ( 'NONE',  ( -50.62287095715005592, -24.99132157543083821, 2.256160258750667502 ) ) ;
#7337=AXIS2_PLACEMENT_3D ( 'NONE', #18591, #42460, #35336 ) ;
#7339=DIRECTION ( 'NONE',  ( -3.773278334453080206E-23, 0.9999999999976377785, 2.173523156925979975E-06 ) ) ;
#7340=CARTESIAN_POINT ( 'NONE',  ( 18.56524475492553705, -13.42312393814442650, -1.500000000000002220 ) ) ;
#7341=CARTESIAN_POINT ( 'NONE',  ( -51.19827071096799642, -25.27420643956589785, 3.666039933461763489 ) ) ;
#7342=CARTESIAN_POINT ( 'NONE',  ( -7.614213781628100364, -20.28429660096114517, -1.500000000000002220 ) ) ;
#7343=CARTESIAN_POINT ( 'NONE',  ( -123.5557606486684676, -23.96119346886881019, -0.6495511937832023630 ) ) ;
#7345=CARTESIAN_POINT ( 'NONE',  ( 20.66465755290784401, -3.126920214821775623, 11.49999999999999645 ) ) ;
#7346=ORIENTED_EDGE ( 'NONE', *, *, #4097, .F. ) ;
#7347=CARTESIAN_POINT ( 'NONE',  ( -69.32616065491644974, -25.31612503761393285, 5.234946770129553784 ) ) ;
#7348=CARTESIAN_POINT ( 'NONE',  ( -6.199593828526920092, 21.14725108817225419, 11.49999999999998934 ) ) ;
#7349=ADVANCED_FACE ( 'NONE', ( #49722 ), #45740, .T. ) ;
#7350=EDGE_CURVE ( 'NONE', #95505, #42298, #43594, .T. ) ;
#7351=CARTESIAN_POINT ( 'NONE',  ( -105.5110081277101983, -24.63419186844610920, 9.035850630976920428 ) ) ;
#7352=CARTESIAN_POINT ( 'NONE',  ( -40.62732473945732181, -25.29087035909526904, 2.839335978436782870 ) ) ;
#7353=VERTEX_POINT ( 'NONE', #5517 ) ;
#7355=DIRECTION ( 'NONE',  ( 0.000000000000000000, 0.9999999999976377785, 2.173523156925979128E-06 ) ) ;
#7357=CARTESIAN_POINT ( 'NONE',  ( -62.52287095715006160, -29.50250243563736774, 8.947779886222145151 ) ) ;
#7358=ORIENTED_EDGE ( 'NONE', *, *, #2614, .F. ) ;
#7360=CARTESIAN_POINT ( 'NONE',  ( -71.59236747742473028, -24.15620529776628445, 10.23563542870660115 ) ) ;
#7361=B_SPLINE_CURVE_WITH_KNOTS ( 'NONE', 3,
 ( #3005, #4985, #33941, #42068, #83592, #46055 ),
 .UNSPECIFIED., .F., .F.,
 ( 4, 2, 4 ),
 ( 6.391158118961560919E-06, 0.001387004593080787230, 0.002767618028042612838 ),
 .UNSPECIFIED. ) ;
#7363=CARTESIAN_POINT ( 'NONE',  ( -36.48447499359400581, -24.51314013834317151, 0.6176544820404150649 ) ) ;
#7364=CARTESIAN_POINT ( 'NONE',  ( -0.3173379506236611580, 20.48240526196808631, -1.500000000000002220 ) ) ;
#7365=ORIENTED_EDGE ( 'NONE', *, *, #37071, .F. ) ;
#7368=CARTESIAN_POINT ( 'NONE',  ( -44.60756723058806017, -23.73766607897669800, -1.055555164236458898 ) ) ;
#7370=CARTESIAN_POINT ( 'NONE',  ( 6.212073114426278408, 21.40951068830820958, 11.49999999999998934 ) ) ;
#7373=CARTESIAN_POINT ( 'NONE',  ( -28.58953762381672092, -24.49418409732524538, 8.947790446961807476 ) ) ;
#7376=CARTESIAN_POINT ( 'NONE',  ( -39.52287095715006160, -23.73934037231757088, 11.05740245334329153 ) ) ;
#7378=CARTESIAN_POINT ( 'NONE',  ( -20.21371806590929410, -4.994250807877889109, -1.500000000000002220 ) ) ;
#7381=ORIENTED_EDGE ( 'NONE', *, *, #47429, .F. ) ;
#7382=CARTESIAN_POINT ( 'NONE',  ( -98.52287095714999055, -23.73934037231757088, 11.05740245334328087 ) ) ;
#7383=ORIENTED_EDGE ( 'NONE', *, *, #60257, .T. ) ;
#7386=LINE ( 'NONE', #24112, #46410 ) ;
#7388=DIRECTION ( 'NONE',  ( 3.773278334444167608E-23, -1.000000000000000000, 0.000000000000000000 ) ) ;
#7389=CARTESIAN_POINT ( 'NONE',  ( -109.6272648782309886, -25.14892542572373202, 2.994947275832184896 ) ) ;
#7391=ADVANCED_FACE ( 'NONE', ( #82641 ), #46586, .T. ) ;
#7392=CARTESIAN_POINT ( 'NONE',  ( -18.93877658415168241, -11.43451605920036052, 11.49999999999999645 ) ) ;
#7393=ORIENTED_EDGE ( 'NONE', *, *, #89661, .T. ) ;
#7396=CARTESIAN_POINT ( 'NONE',  ( 20.10346781357453949, 10.43426432342431553, -1.500000000000002220 ) ) ;
#7397=CARTESIAN_POINT ( 'NONE',  ( -29.23546583316962710, -25.19426066751507065, 5.521667863429778222 ) ) ;
#7398=ORIENTED_EDGE ( 'NONE', *, *, #77021, .T. ) ;
#7400=CARTESIAN_POINT ( 'NONE',  ( -57.55620429048340725, -23.47596703998600276, 11.44779298504227505 ) ) ;
#7401=EDGE_CURVE ( 'NONE', #72936, #99871, #52193, .T. ) ;
#7402=B_SPLINE_CURVE_WITH_KNOTS ( 'NONE', 3,
 ( #43358, #20990, #45351, #4786 ),
 .UNSPECIFIED., .F., .F.,
 ( 4, 4 ),
 ( 0.000000000000000000, 9.999999999998897304E-05 ),
 .UNSPECIFIED. ) ;
#7403=CARTESIAN_POINT ( 'NONE',  ( -17.82723130383223165, -9.322377578706960932, -1.500000000000002220 ) ) ;
#7404=ADVANCED_FACE ( 'NONE', ( #59826 ), #400, .T. ) ;
#7407=VECTOR ( 'NONE', #90643, 1000.000000000000114 ) ;
#7409=CARTESIAN_POINT ( 'NONE',  ( -2.124831620219566730, 22.23837930986240607, -1.500000000000002220 ) ) ;
#7413=ORIENTED_EDGE ( 'NONE', *, *, #7498, .T. ) ;
#7414=VERTEX_POINT ( 'NONE', #61825 ) ;
#7415=CARTESIAN_POINT ( 'NONE',  ( -101.2134684488937069, -25.25341235495022474, 6.841542769133510227 ) ) ;
#7416=DIRECTION ( 'NONE',  ( 0.000000000000000000, 2.173523156925980399E-06, -0.9999999999976378895 ) ) ;
#7422=CARTESIAN_POINT ( 'NONE',  ( -8.292788067677484776, 17.68049324621676632, -1.500000000000002220 ) ) ;
#7423=CARTESIAN_POINT ( 'NONE',  ( -38.62287095715005592, -23.47596703998600276, 11.44779298504227505 ) ) ;
#7424=CARTESIAN_POINT ( 'NONE',  ( 11.86944616785735818, -17.87650476368427732, -1.500000000000002220 ) ) ;
#7425=CARTESIAN_POINT ( 'NONE',  ( -25.53098197642538736, -24.58000217321816194, 4.942812437106832490 ) ) ;
#7426=LINE ( 'NONE', #6934, #71374 ) ;
#7427=CARTESIAN_POINT ( 'NONE',  ( -126.6228709571500559, -29.50247984919015209, -1.443849546365044922 ) ) ;
#7428=CARTESIAN_POINT ( 'NONE',  ( 2.875404258304424143, 22.71175023210845012, -1.500000000000002220 ) ) ;
#7430=CARTESIAN_POINT ( 'NONE',  ( -104.6228709571500559, -24.66019654487200086, 8.947790411086124607 ) ) ;
#7431=CARTESIAN_POINT ( 'NONE',  ( -108.5228709571500758, -24.51283580621449687, 0.6167428607045382094 ) ) ;
#7432=CARTESIAN_POINT ( 'NONE',  ( 2.879247915899910470, -19.84986158617241614, 11.49999999999999645 ) ) ;
#7433=CARTESIAN_POINT ( 'NONE',  ( -79.34156256387794315, -25.31594405533091674, 4.917719298043063958 ) ) ;
#7434=CARTESIAN_POINT ( 'NONE',  ( -64.55620429048339304, -24.64898659630529210, 1.056161002820825923 ) ) ;
#7436=CARTESIAN_POINT ( 'NONE',  ( -104.5228709571500758, -29.50250243563736774, 8.947779886222138046 ) ) ;
#7437=ORIENTED_EDGE ( 'NONE', *, *, #52311, .T. ) ;
#7438=CARTESIAN_POINT ( 'NONE',  ( -26.36100103624393753, -24.65813067085167631, 2.183744232383703299 ) ) ;
#7440=CARTESIAN_POINT ( 'NONE',  ( 1.329761939549756855, 21.69843865049760367, -1.500000000000002220 ) ) ;
#7442=CARTESIAN_POINT ( 'NONE',  ( 5.347671334029483248, -18.86178030415664963, -1.500000000000002220 ) ) ;
#7443=LINE ( 'NONE', #76947, #55581 ) ;
#7445=CARTESIAN_POINT ( 'NONE',  ( -109.6235167689328591, -25.27925821723561128, 4.923693497153672993 ) ) ;
#7447=CARTESIAN_POINT ( 'NONE',  ( -124.5228709571500616, -29.50248528299804818, 1.056150453629045360 ) ) ;
#7448=CARTESIAN_POINT ( 'NONE',  ( -47.52287095715006160, -24.50321055353805377, 9.387540953477525818 ) ) ;
#7449=CARTESIAN_POINT ( 'NONE',  ( 19.83930831332124001, -5.160774681608516268, 11.49999999999999645 ) ) ;
#7450=CARTESIAN_POINT ( 'NONE',  ( -94.52287095715004739, -24.50216790748205042, 0.6166512839542538371 ) ) ;
#7451=CARTESIAN_POINT ( 'NONE',  ( -120.6253545820920294, -24.52300882791530512, 0.6510814631126412566 ) ) ;
#7456=CARTESIAN_POINT ( 'NONE',  ( -125.5551857379501541, -24.40133493613050675, 9.663955038902798833 ) ) ;
#7457=DIRECTION ( 'NONE',  ( 0.000000000000000000, -2.173523156925979552E-06, 0.9999999999976378895 ) ) ;
#7460=VECTOR ( 'NONE', #60259, 1000.000000000000114 ) ;
#7461=B_SPLINE_CURVE_WITH_KNOTS ( 'NONE', 3,
 ( #74200, #35641, #12781, #90914 ),
 .UNSPECIFIED., .F., .F.,
 ( 4, 4 ),
 ( 0.000000000000000000, 1.000000000000000000 ),
 .UNSPECIFIED. ) ;
#7462=CARTESIAN_POINT ( 'NONE',  ( 16.10802587768190008, -16.50329280669357246, 11.49999999999999645 ) ) ;
#7463=CARTESIAN_POINT ( 'NONE',  ( 22.53581206741051446, 3.480912172000575122, 11.49999999999998934 ) ) ;
#7464=CARTESIAN_POINT ( 'NONE',  ( -125.6228709571500843, -25.00158670708909625, 2.256160236439166855 ) ) ;
#7465=FACE_OUTER_BOUND ( 'NONE', #29334, .T. ) ;
#7467=CARTESIAN_POINT ( 'NONE',  ( 21.53444271425275858, 6.169869319618734416, 11.49999999999999645 ) ) ;
#7468=ORIENTED_EDGE ( 'NONE', *, *, #93457, .T. ) ;
#7471=CARTESIAN_POINT ( 'NONE',  ( -16.24880213243413607, 14.73142910551002238, -1.500000000000002220 ) ) ;
#7476=CARTESIAN_POINT ( 'NONE',  ( -34.52287095715004739, -24.66019654487199730, 8.947790411086121054 ) ) ;
#7478=CARTESIAN_POINT ( 'NONE',  ( -117.6228709571500559, -23.94994826722515668, -0.6494450866351687557 ) ) ;
#7481=CARTESIAN_POINT ( 'NONE',  ( -9.379331868514380943, 18.20734191464070406, 11.49999999999998934 ) ) ;
#7483=VECTOR ( 'NONE', #33095, 1000.000000000000114 ) ;
#7484=EDGE_LOOP ( 'NONE', ( #68401, #7116, #10610, #77647 ) ) ;
#7486=B_SPLINE_CURVE_WITH_KNOTS ( 'NONE', 3,
 ( #624, #32573, #55932, #63554 ),
 .UNSPECIFIED., .F., .F.,
 ( 4, 4 ),
 ( 2.775557561562891043E-17, 9.999999999998898659E-05 ),
 .UNSPECIFIED. ) ;
#7487=VERTEX_POINT ( 'NONE', #46596 ) ;
#7488=CARTESIAN_POINT ( 'NONE',  ( -23.05830607064937965, -0.9945063503333604338, 11.49999999999998934 ) ) ;
#7489=DIRECTION ( 'NONE',  ( -3.773278334453079618E-23, 0.9999999999976377785, 2.173523156925979975E-06 ) ) ;
#7490=CARTESIAN_POINT ( 'NONE',  ( -18.77428246231291808, -7.638711222589018135, -1.500000000000002220 ) ) ;
#7492=EDGE_LOOP ( 'NONE', ( #57604, #23239, #76064, #44842 ) ) ;
#7494=CARTESIAN_POINT ( 'NONE',  ( -90.55620429048337883, -25.00182538069145721, 7.747789668545099317 ) ) ;
#7496=CARTESIAN_POINT ( 'NONE',  ( -127.5895376238166961, -24.64965694238408034, 8.947790433994645909 ) ) ;
#7498=EDGE_CURVE ( 'NONE', #40585, #51301, #39478, .T. ) ;
#7500=CARTESIAN_POINT ( 'NONE',  ( -70.60486894837754335, -23.85016227208580730, -0.8807180028928335291 ) ) ;
#7501=CARTESIAN_POINT ( 'NONE',  ( -21.12015818079280649, -3.594773940630530795, 11.49999999999999645 ) ) ;
#7503=CARTESIAN_POINT ( 'NONE',  ( -75.49320323011643552, -24.83618233451450763, 1.606449574219540599 ) ) ;
#7504=LINE ( 'NONE', #14109, #66921 ) ;
#7505=EDGE_CURVE ( 'NONE', #72155, #88376, #53714, .T. ) ;
#7507=CARTESIAN_POINT ( 'NONE',  ( -0.2510023010970363067, -20.70922355669356563, 11.49999999999998934 ) ) ;
#7508=ORIENTED_EDGE ( 'NONE', *, *, #18593, .T. ) ;
#7511=CARTESIAN_POINT ( 'NONE',  ( -102.6228709571500559, -23.47593901973091235, -1.443836447539001089 ) ) ;
#7512=ORIENTED_EDGE ( 'NONE', *, *, #44637, .T. ) ;
#7513=EDGE_LOOP ( 'NONE', ( #86537, #61319, #9067, #31998 ) ) ;
#7515=PLANE ( 'NONE',  #74066 ) ;
#7516=CARTESIAN_POINT ( 'NONE',  ( -65.62787674017165784, -24.83618233451449697, 1.606449574219540155 ) ) ;
#7518=CARTESIAN_POINT ( 'NONE',  ( -20.77788740438921522, -7.151594987469691134, 11.49999999999999645 ) ) ;
#7519=CARTESIAN_POINT ( 'NONE',  ( -89.62850461461094653, -24.35071581493543391, 9.817618358456025263 ) ) ;
#7520=CARTESIAN_POINT ( 'NONE',  ( 17.82461400791848405, -13.82690402418615960, -1.500000000000002220 ) ) ;
#7522=CARTESIAN_POINT ( 'NONE',  ( -18.73635099073748833, 9.434554061794083069, 11.49999999999998934 ) ) ;
#7527=VERTEX_POINT ( 'NONE', #72937 ) ;
#7529=CARTESIAN_POINT ( 'NONE',  ( -112.5228709571500616, -24.65952944569304961, 1.056160979905704123 ) ) ;
#7530=B_SPLINE_CURVE_WITH_KNOTS ( 'NONE', 3,
 ( #2077, #45007, #81687, #19273, #66491, #97404 ),
 .UNSPECIFIED., .F., .F.,
 ( 4, 2, 4 ),
 ( 6.384118678612105596E-06, 0.001386860460828374117, 0.002767336802978135821 ),
 .UNSPECIFIED. ) ;
#7532=B_SPLINE_CURVE_WITH_KNOTS ( 'NONE', 3,
 ( #31228, #63711, #17507, #39841 ),
 .UNSPECIFIED., .F., .F.,
 ( 4, 4 ),
 ( 0.000000000000000000, 9.999999999999591193E-05 ),
 .UNSPECIFIED. ) ;
#7533=CARTESIAN_POINT ( 'NONE',  ( 7.367719877546908158, -20.20905560389912026, -1.500000000000002220 ) ) ;
#7535=ORIENTED_EDGE ( 'NONE', *, *, #96338, .T. ) ;
#7536=CARTESIAN_POINT ( 'NONE',  ( 0.3207198112191017025, -21.10926996749724083, 11.49999999999998934 ) ) ;
#7537=DIRECTION ( 'NONE',  ( 3.773278334444167608E-23, -1.000000000000000000, 0.000000000000000000 ) ) ;
#7538=CARTESIAN_POINT ( 'NONE',  ( -60.73059407482809036, -25.14083923594472125, 2.947789366366679875 ) ) ;
#7540=CARTESIAN_POINT ( 'NONE',  ( -89.52287095715006160, -29.50250243563736774, 8.947779886222139822 ) ) ;
#7541=LINE ( 'NONE', #55737, #76186 ) ;
#7542=CARTESIAN_POINT ( 'NONE',  ( 14.67205787815721862, 16.58792043909384262, -1.500000000000002220 ) ) ;
#7543=CARTESIAN_POINT ( 'NONE',  ( -71.63072430240342214, -24.34968618360933945, 0.1864209137778822800 ) ) ;
#7544=EDGE_CURVE ( 'NONE', #21016, #91623, #68014, .T. ) ;
#7545=ORIENTED_EDGE ( 'NONE', *, *, #16805, .F. ) ;
#7551=CARTESIAN_POINT ( 'NONE',  ( -100.5087677528688062, -24.63355581998385091, 0.9682620441943978751 ) ) ;
#7552=EDGE_CURVE ( 'NONE', #62807, #896, #59572, .T. ) ;
#7553=CARTESIAN_POINT ( 'NONE',  ( -7.499459838998954631, -17.95702976299720532, -1.500000000000002220 ) ) ;
#7554=CARTESIAN_POINT ( 'NONE',  ( -18.12654925440673637, -11.31956730046968751, 11.49999999999998934 ) ) ;
#7555=CARTESIAN_POINT ( 'NONE',  ( -68.93918693012690824, -25.25799956426409665, 6.184868438663939649 ) ) ;
#7556=CARTESIAN_POINT ( 'NONE',  ( -106.6228709571500559, -23.48783264082479150, -1.443836473390060382 ) ) ;
#7558=LINE ( 'NONE', #55253, #89762 ) ;
#7559=CARTESIAN_POINT ( 'NONE',  ( -22.35490716430079061, -3.811827842488555440, -1.500000000000002220 ) ) ;
#7560=VECTOR ( 'NONE', #98553, 1000.000000000000114 ) ;
#7564=CARTESIAN_POINT ( 'NONE',  ( 17.16143643543069075, 9.858047367376444825, 11.49999999999999645 ) ) ;
#7567=EDGE_LOOP ( 'NONE', ( #41051, #39856, #88816, #95732 ) ) ;
#7570=CARTESIAN_POINT ( 'NONE',  ( -71.52287095715007581, -24.64965694238408034, 8.947790433994200043 ) ) ;
#7571=CARTESIAN_POINT ( 'NONE',  ( 21.56569437331729233, -1.927008741106717604, 11.49999999999998934 ) ) ;
#7572=CARTESIAN_POINT ( 'NONE',  ( -66.58953762381672448, -24.65952944569304606, 1.056160979905694131 ) ) ;
#7573=CARTESIAN_POINT ( 'NONE',  ( -19.39930850525863804, 0.8904154686948315689, -1.500000000000002220 ) ) ;
#7575=CARTESIAN_POINT ( 'NONE',  ( -80.52287095715006160, -24.15516710230293995, 10.28746687063725851 ) ) ;
#7576=CARTESIAN_POINT ( 'NONE',  ( -55.48002222786107041, -24.92592662359561118, 8.075495903017996469 ) ) ;
#7577=CARTESIAN_POINT ( 'NONE',  ( 12.34629653512297409, 15.52844579862587437, 11.49999999999998934 ) ) ;
#7578=EDGE_LOOP ( 'NONE', ( #15889, #49427, #3170, #75376 ) ) ;
#7579=CARTESIAN_POINT ( 'NONE',  ( -18.82647582233506611, 7.659846263794035437, 11.49999999999999645 ) ) ;
#7580=CARTESIAN_POINT ( 'NONE',  ( -80.63078619424426563, -24.63355581998386157, 0.9682620441943954326 ) ) ;
#7581=LINE ( 'NONE', #84698, #2027 ) ;
#7583=CARTESIAN_POINT ( 'NONE',  ( -102.5854978320862045, -24.66019654487200086, 8.947790411086115725 ) ) ;
#7585=CARTESIAN_POINT ( 'NONE',  ( -96.62287095715005592, -24.33927499327854704, 9.819080762295817166 ) ) ;
#7586=CARTESIAN_POINT ( 'NONE',  ( -40.52986559551381873, -24.73531770709094957, 8.716586749053510275 ) ) ;
#7588=CARTESIAN_POINT ( 'NONE',  ( -18.81522532469529452, 6.996975221643539911, 11.49999999999998934 ) ) ;
#7589=CARTESIAN_POINT ( 'NONE',  ( -85.52287095715010423, -24.82558206586148941, 1.605769216559626678 ) ) ;
#7593=CARTESIAN_POINT ( 'NONE',  ( -21.74799678179195794, 7.114197580472080951, 11.49999999999999645 ) ) ;
#7594=CARTESIAN_POINT ( 'NONE',  ( 9.518656604726816184, -20.62229310799655124, 11.49999999999998934 ) ) ;
#7595=ORIENTED_EDGE ( 'NONE', *, *, #43839, .F. ) ;
#7596=CARTESIAN_POINT ( 'NONE',  ( -30.47287095715007865, -24.48302893026593452, 9.401871521831095535 ) ) ;
#7598=CARTESIAN_POINT ( 'NONE',  ( -39.96950833219506904, -25.20884380724118401, 3.393814871506949604 ) ) ;
#7599=CARTESIAN_POINT ( 'NONE',  ( -73.62287095715005592, -23.48783264082478084, -1.443836473390067487 ) ) ;
#7600=CARTESIAN_POINT ( 'NONE',  ( -128.5553789593330976, -24.66019654487200441, 8.947790411086112172 ) ) ;
#7601=B_SPLINE_CURVE_WITH_KNOTS ( 'NONE', 3,
 ( #40979, #26251, #50098, #97256, #33352, #95758 ),
 .UNSPECIFIED., .F., .F.,
 ( 4, 2, 4 ),
 ( 1.570887131794795405E-05, 0.001396322306279761940, 0.002776935741241575838 ),
 .UNSPECIFIED. ) ;
#7602=CARTESIAN_POINT ( 'NONE',  ( -44.52287095715006160, -29.50248528299804818, 1.056150453629031594 ) ) ;
#7603=ORIENTED_EDGE ( 'NONE', *, *, #34567, .F. ) ;
#7604=EDGE_CURVE ( 'NONE', #17917, #70388, #30437, .T. ) ;
#7605=CARTESIAN_POINT ( 'NONE',  ( 11.27307661227339430, 16.98952936956587934, 11.49999999999998934 ) ) ;
#7606=VERTEX_POINT ( 'NONE', #42500 ) ;
#7608=CARTESIAN_POINT ( 'NONE',  ( 14.37299948674089123, 17.95305339730678185, 11.49999999999998934 ) ) ;
#7609=B_SPLINE_CURVE_WITH_KNOTS ( 'NONE', 3,
 ( #78671, #57388, #40645, #65005 ),
 .UNSPECIFIED., .F., .F.,
 ( 4, 4 ),
 ( 0.000000000000000000, 9.999999999998897304E-05 ),
 .UNSPECIFIED. ) ;
#7611=ADVANCED_FACE ( 'NONE', ( #57719 ), #69240, .T. ) ;
#7612=EDGE_LOOP ( 'NONE', ( #45086, #26156, #34346, #90365 ) ) ;
#7614=ADVANCED_FACE ( 'NONE', ( #2933 ), #22222, .T. ) ;
#7617=EDGE_CURVE ( 'NONE', #86729, #13348, #82529, .T. ) ;
#7618=CARTESIAN_POINT ( 'NONE',  ( -51.53189091124832544, -24.66019654487199730, 8.947790411086117501 ) ) ;
#7619=CARTESIAN_POINT ( 'NONE',  ( 20.85495618715548716, -4.085033163991189653, 11.49999999999999645 ) ) ;
#7620=ORIENTED_EDGE ( 'NONE', *, *, #31195, .T. ) ;
#7622=CARTESIAN_POINT ( 'NONE',  ( 22.14152233036116257, 1.636640089565777334, -1.500000000000002220 ) ) ;
#7623=B_SPLINE_CURVE_WITH_KNOTS ( 'NONE', 3,
 ( #93894, #24382, #78649, #24878, #9156, #40116 ),
 .UNSPECIFIED., .F., .F.,
 ( 4, 2, 4 ),
 ( 0.000000000000000000, 0.001380764517854764749, 0.002761529035709529498 ),
 .UNSPECIFIED. ) ;
#7624=CARTESIAN_POINT ( 'NONE',  ( -18.80638259998596951, 8.471300643254643603, -1.500000000000002220 ) ) ;
#7625=AXIS2_PLACEMENT_3D ( 'NONE', #24323, #69999, #486 ) ;
#7629=CARTESIAN_POINT ( 'NONE',  ( -39.08636289603285974, -25.26169826439894806, 3.855163135067930735 ) ) ;
#7632=CARTESIAN_POINT ( 'NONE',  ( -91.54631484340760039, -24.51314013834315375, 0.6176544820404143987 ) ) ;
#7633=AXIS2_PLACEMENT_3D ( 'NONE', #11769, #5160, #42743 ) ;
#7634=VERTEX_POINT ( 'NONE', #81548 ) ;
#7637=CARTESIAN_POINT ( 'NONE',  ( -18.77111393065419875, 9.022841878967760465, -1.500000000000002220 ) ) ;
#7639=CARTESIAN_POINT ( 'NONE',  ( -21.76810506448615712, 0.6044244127108716613, 11.49999999999999645 ) ) ;
#7641=CARTESIAN_POINT ( 'NONE',  ( -78.54307297471228821, -24.51419770103157347, 9.386484678747175181 ) ) ;
#7642=CARTESIAN_POINT ( 'NONE',  ( -22.32441756149717094, -2.617931739244098388, -1.500000000000002220 ) ) ;
#7644=VERTEX_POINT ( 'NONE', #74907 ) ;
#7646=CARTESIAN_POINT ( 'NONE',  ( -51.52287095715006870, -29.50248528299804818, 1.056150453629033370 ) ) ;
#7648=ORIENTED_EDGE ( 'NONE', *, *, #52348, .F. ) ;
#7649=ORIENTED_EDGE ( 'NONE', *, *, #34556, .F. ) ;
#7650=ORIENTED_EDGE ( 'NONE', *, *, #24822, .T. ) ;
#7651=CARTESIAN_POINT ( 'NONE',  ( 16.79701800048795590, -13.18750964578662455, -1.500000000000002220 ) ) ;
#7653=CARTESIAN_POINT ( 'NONE',  ( 12.99892964944760543, 16.54660993828877125, 11.49999999999998934 ) ) ;
#7654=CARTESIAN_POINT ( 'NONE',  ( -30.53944614433371640, -24.75758798069637123, 1.363670884829966123 ) ) ;
#7655=CARTESIAN_POINT ( 'NONE',  ( -99.52764846858842418, -25.26416398485831749, 3.999772271414141489 ) ) ;
#7656=CARTESIAN_POINT ( 'NONE',  ( -28.62287095715004881, -23.31957264754183967, 11.44779298504227860 ) ) ;
#7657=CARTESIAN_POINT ( 'NONE',  ( 2.959355296939036872, -21.81356824310248399, -1.500000000000002220 ) ) ;
#7658=DIRECTION ( 'NONE',  ( 0.000000000000000000, -0.9999999999976377785, -2.173523156925979128E-06 ) ) ;
#7660=CARTESIAN_POINT ( 'NONE',  ( -65.62370081105176212, -25.00182538069147142, 7.747789668545043362 ) ) ;
#7662=VECTOR ( 'NONE', #65097, 1000.000000000000114 ) ;
#7663=EDGE_CURVE ( 'NONE', #11406, #49490, #67320, .T. ) ;
#7667=CARTESIAN_POINT ( 'NONE',  ( -0.04482400408598174318, -22.46971804258298633, 8.370978854367624677 ) ) ;
#7668=CARTESIAN_POINT ( 'NONE',  ( -12.14505723179402530, 17.47690347785001919, -1.500000000000002220 ) ) ;
#7669=FACE_OUTER_BOUND ( 'NONE', #14096, .T. ) ;
#7670=CARTESIAN_POINT ( 'NONE',  ( -107.5594716292221449, -23.48786465467241769, 11.44779295918253936 ) ) ;
#7674=CARTESIAN_POINT ( 'NONE',  ( -0.06565682164858396841, -22.51586213336150166, -1.500000000000002220 ) ) ;
#7675=B_SPLINE_SURFACE_WITH_KNOTS ( 'NONE', 3, 3, ( 
 ( #14757, #22359, #99982, #37611 ),
 ( #68563, #90897, #75655, #91886 ),
 ( #45726, #76649, #60961, #59457 ),
 ( #43734, #37109, #91388, #99494 ),
 ( #36116, #30491, #29989, #74668 ),
 ( #53348, #5165, #67577, #68071 ),
 ( #84275, #83280, #29486, #61460 ) ),
 .UNSPECIFIED., .F., .F., .F.,
 ( 4, 3, 4 ),
 ( 4, 4 ),
 ( 0.0004766839783843789826, 0.1029713700210909827, 0.2054660560637975864 ),
 ( 0.4296032809832535659, 0.4308142237037666522 ),
 .UNSPECIFIED. ) ;
#7677=ORIENTED_EDGE ( 'NONE', *, *, #3122, .F. ) ;
#7678=CARTESIAN_POINT ( 'NONE',  ( -79.71056221673293862, -25.30034170514263892, 4.643640274121591638 ) ) ;
#7679=CARTESIAN_POINT ( 'NONE',  ( 18.24227566675094181, -7.298356753547692755, 11.49999999999999645 ) ) ;
#7680=CARTESIAN_POINT ( 'NONE',  ( -55.55620429048338593, -25.00182538069145011, 7.747789668545099317 ) ) ;
#7682=ORIENTED_EDGE ( 'NONE', *, *, #86241, .T. ) ;
#7683=CARTESIAN_POINT ( 'NONE',  ( -50.52287095715006160, -23.48783264082477018, -1.443836473390095021 ) ) ;
#7684=CARTESIAN_POINT ( 'NONE',  ( -126.1692191815178319, -25.31364695005282428, 6.500946884335763620 ) ) ;
#7685=CARTESIAN_POINT ( 'NONE',  ( -90.93633033381745179, -25.06732983082694233, 7.447789526168957508 ) ) ;
#7687=CARTESIAN_POINT ( 'NONE',  ( 19.26447527235507451, 4.322997736827044690, 11.49999999999998934 ) ) ;
#7690=CARTESIAN_POINT ( 'NONE',  ( -70.62287095715001328, -24.92579138211020862, 1.929029949965668456 ) ) ;
#7691=VECTOR ( 'NONE', #37680, 1000.000000000000114 ) ;
#7694=EDGE_LOOP ( 'NONE', ( #47699, #58568, #11614, #54187 ) ) ;
#7695=CARTESIAN_POINT ( 'NONE',  ( -45.92287095715006728, -23.47593901973090880, -1.443836447538998202 ) ) ;
#7696=LINE ( 'NONE', #8204, #42593 ) ;
#7697=CARTESIAN_POINT ( 'NONE',  ( -88.52287095715006160, -24.64965694238407323, 8.947790433994196491 ) ) ;
#7698=CARTESIAN_POINT ( 'NONE',  ( -69.55126625704997423, -29.50248967467915051, 3.076686136236004732 ) ) ;
#7701=CARTESIAN_POINT ( 'NONE',  ( -56.58953762381673158, -24.65952944569303895, 1.056160979905694575 ) ) ;
#7702=CARTESIAN_POINT ( 'NONE',  ( -43.58953762381671737, -23.48786465467241058, 11.44779295918255180 ) ) ;
#7703=CARTESIAN_POINT ( 'NONE',  ( -19.95465934538571062, -0.7993260556091378310, -1.500000000000002220 ) ) ;
#7705=CARTESIAN_POINT ( 'NONE',  ( -51.22152257355241289, -25.31467655261325334, 4.840581831727154061 ) ) ;
#7706=EDGE_LOOP ( 'NONE', ( #84740, #66784, #19809, #8181 ) ) ;
#7707=CARTESIAN_POINT ( 'NONE',  ( -79.54332137893563015, -24.51419770103157347, 9.386484678747176957 ) ) ;
#7708=CARTESIAN_POINT ( 'NONE',  ( -109.7130628311247591, -25.29012770170046309, 3.499763135497069744 ) ) ;
#7709=CARTESIAN_POINT ( 'NONE',  ( -58.52287095715009713, -24.66019654487199730, 8.947790411086121054 ) ) ;
#7710=CARTESIAN_POINT ( 'NONE',  ( -108.5228709571500616, -24.64898659630528854, 1.056161002820831474 ) ) ;
#7711=CARTESIAN_POINT ( 'NONE',  ( -27.85310647731327904, -24.60093890951422679, 1.631228552719281577 ) ) ;
#7712=CARTESIAN_POINT ( 'NONE',  ( -83.51347087090108801, -23.96119346886880663, -0.6495511937832110227 ) ) ;
#7713=PLANE ( 'NONE',  #44692 ) ;
#7714=LINE ( 'NONE', #84332, #43688 ) ;
#7715=ORIENTED_EDGE ( 'NONE', *, *, #89580, .T. ) ;
#7718=CARTESIAN_POINT ( 'NONE',  ( -15.58492919356500650, -12.95507736684500699, 11.49999999999998934 ) ) ;
#7719=CARTESIAN_POINT ( 'NONE',  ( -49.62287095715005592, -23.48786465467241058, 11.44779295918254824 ) ) ;
#7720=ADVANCED_FACE ( 'NONE', ( #35376 ), #73930, .F. ) ;
#7723=EDGE_CURVE ( 'NONE', #11910, #73893, #82558, .T. ) ;
#7724=ORIENTED_EDGE ( 'NONE', *, *, #33510, .F. ) ;
#7725=LINE ( 'NONE', #36684, #87422 ) ;
#7726=CARTESIAN_POINT ( 'NONE',  ( 14.24339680280927567, 14.23919408161895284, -1.500000000000002220 ) ) ;
#7727=ADVANCED_FACE ( 'NONE', ( #52585 ), #14008, .F. ) ;
#7728=CARTESIAN_POINT ( 'NONE',  ( -19.04630365209304799, -9.011775662611203330, 11.49999999999999645 ) ) ;
#7729=CARTESIAN_POINT ( 'NONE',  ( -18.93877658415168241, -11.43451605920036052, 11.49999999999998934 ) ) ;
#7730=EDGE_CURVE ( 'NONE', #38181, #41241, #90152, .T. ) ;
#7731=CARTESIAN_POINT ( 'NONE',  ( -10.66544979547405347, 17.54311462378693420, 11.49999999999998934 ) ) ;
#7732=LINE ( 'NONE', #56818, #81946 ) ;
#7735=CARTESIAN_POINT ( 'NONE',  ( -36.52287095715006870, -29.50248528299804818, 1.056150453629031594 ) ) ;
#7736=ORIENTED_EDGE ( 'NONE', *, *, #54021, .F. ) ;
#7737=CARTESIAN_POINT ( 'NONE',  ( -51.62287095715007723, -23.94994826722565762, -0.6494450866342734718 ) ) ;
#7738=CARTESIAN_POINT ( 'NONE',  ( -85.62287095715008434, -24.83620972994592080, 8.398175272781367440 ) ) ;
#7739=ORIENTED_EDGE ( 'NONE', *, *, #13208, .F. ) ;
#7743=CARTESIAN_POINT ( 'NONE',  ( -63.62287095715004881, -24.34917612406837861, 0.1852690917426589035 ) ) ;
#7745=CARTESIAN_POINT ( 'NONE',  ( 4.765357849511589805, 20.07956653139741121, -1.500000000000002220 ) ) ;
#7746=CARTESIAN_POINT ( 'NONE',  ( -16.54959454218438708, 13.92943311328891554, 11.49999999999999645 ) ) ;
#7747=ORIENTED_EDGE ( 'NONE', *, *, #64519, .F. ) ;
#7748=DIRECTION ( 'NONE',  ( 0.000000000000000000, -0.9999999999976377785, -2.173523156925979128E-06 ) ) ;
#7749=CARTESIAN_POINT ( 'NONE',  ( -57.62287095715004881, -24.50321055353805022, 9.387540953477532923 ) ) ;
#7750=CARTESIAN_POINT ( 'NONE',  ( 0.3464652362752086434, -22.36268665536068667, -1.500000000000002220 ) ) ;
#7753=CARTESIAN_POINT ( 'NONE',  ( -79.47715298469661604, -25.12205682912399141, 6.508607931329533969 ) ) ;
#7754=CARTESIAN_POINT ( 'NONE',  ( -74.92287095715006728, -23.47596703998600631, 11.44779298504227860 ) ) ;
#7756=CARTESIAN_POINT ( 'NONE',  ( -99.53743757535663406, -25.28407026395041868, 4.125266664010103668 ) ) ;
#7757=CARTESIAN_POINT ( 'NONE',  ( -49.50095828120969799, -24.15620529776627379, 10.23563542870661003 ) ) ;
#7758=FACE_OUTER_BOUND ( 'NONE', #71089, .T. ) ;
#7759=CARTESIAN_POINT ( 'NONE',  ( -19.94816486946033507, 6.322790147265108018, 11.49999999999998934 ) ) ;
#7761=CARTESIAN_POINT ( 'NONE',  ( -98.62287095715008434, -24.50216790748097040, 0.6166512839513733635 ) ) ;
#7763=ORIENTED_EDGE ( 'NONE', *, *, #65280, .F. ) ;
#7764=CARTESIAN_POINT ( 'NONE',  ( -128.6228709571500417, -23.72773821059536559, 11.05748984161097326 ) ) ;
#7765=CARTESIAN_POINT ( 'NONE',  ( 20.98173926746349238, 2.650078317256617577, -1.500000000000002220 ) ) ;
#7766=VERTEX_POINT ( 'NONE', #54585 ) ;
#7767=LINE ( 'NONE', #93494, #51110 ) ;
#7768=CARTESIAN_POINT ( 'NONE',  ( -100.4005007646339891, -25.26221318079232603, 7.100843378255928151 ) ) ;
#7769=CARTESIAN_POINT ( 'NONE',  ( 17.22188757068894915, 13.35947340969901198, 11.49999999999998934 ) ) ;
#7773=CARTESIAN_POINT ( 'NONE',  ( -79.91092262079529007, -25.15690873672783923, 6.961915921126503370 ) ) ;
#7774=CARTESIAN_POINT ( 'NONE',  ( -19.95566455537076678, 8.849265345510103131, -1.500000000000002220 ) ) ;
#7775=CARTESIAN_POINT ( 'NONE',  ( -30.57287095715004099, -23.47593903913510260, -1.434903445928520149 ) ) ;
#7778=CARTESIAN_POINT ( 'NONE',  ( -72.52287095715007581, -24.65952944569304606, 1.056160979905697239 ) ) ;
#7780=ORIENTED_EDGE ( 'NONE', *, *, #68614, .T. ) ;
#7782=ORIENTED_EDGE ( 'NONE', *, *, #50163, .F. ) ;
#7784=CARTESIAN_POINT ( 'NONE',  ( 19.29917393477590437, 8.764703196630867055, 11.49999999999998934 ) ) ;
#7785=CARTESIAN_POINT ( 'NONE',  ( -94.59719327492638286, -23.73766607897670866, -1.055555164236451349 ) ) ;
#7786=CARTESIAN_POINT ( 'NONE',  ( -79.53726446675389639, -25.27791906091428231, 7.255560248500635190 ) ) ;
#7789=CARTESIAN_POINT ( 'NONE',  ( 12.39309347844599252, 14.90900669795185252, -1.500000000000002220 ) ) ;
#7791=EDGE_CURVE ( 'NONE', #32600, #11368, #38878, .T. ) ;
#7792=CARTESIAN_POINT ( 'NONE',  ( -41.88608634761866512, -25.31392318313163514, 5.203682277190879724 ) ) ;
#7794=B_SPLINE_CURVE_WITH_KNOTS ( 'NONE', 3,
 ( #9176, #61978, #8687, #22876 ),
 .UNSPECIFIED., .F., .F.,
 ( 4, 4 ),
 ( 0.6802716898399019385, 0.6892781211120175833 ),
 .UNSPECIFIED. ) ;
#7795=CARTESIAN_POINT ( 'NONE',  ( 11.34002819025610087, 15.78594478779102950, 11.49999999999999645 ) ) ;
#7796=CARTESIAN_POINT ( 'NONE',  ( -76.52287095715007581, -29.50250786944525672, 11.44777988621623521 ) ) ;
#7797=CARTESIAN_POINT ( 'NONE',  ( -84.55620429048339304, -24.65952944569304606, 1.056160979905699460 ) ) ;
#7798=ADVANCED_FACE ( 'NONE', ( #30234 ), #46974, .T. ) ;
#7799=ORIENTED_EDGE ( 'NONE', *, *, #77588, .F. ) ;
#7800=PLANE ( 'NONE',  #70111 ) ;
#7801=DIRECTION ( 'NONE',  ( 3.773278334444167608E-23, -1.000000000000000000, 0.000000000000000000 ) ) ;
#7803=CARTESIAN_POINT ( 'NONE',  ( -93.51856267089354446, -23.73791477778911840, 11.05961554403170410 ) ) ;
#7804=CARTESIAN_POINT ( 'NONE',  ( -18.14765110722914798, -7.448729197826248871, -1.500000000000002220 ) ) ;
#7806=CARTESIAN_POINT ( 'NONE',  ( -117.6228709571500559, -23.48786465467241769, 11.44779295918253759 ) ) ;
#7808=CARTESIAN_POINT ( 'NONE',  ( 17.73057777116804701, 12.32922261165129285, -1.500000000000002220 ) ) ;
#7809=DIRECTION ( 'NONE',  ( 1.000000000000000000, 3.773278334444167608E-23, 8.201307833595939069E-29 ) ) ;
#7810=CARTESIAN_POINT ( 'NONE',  ( -40.58503138813161115, -24.63355581998383670, 0.9682620441943914358 ) ) ;
#7811=CARTESIAN_POINT ( 'NONE',  ( -65.55620429048339304, -25.00182538069145011, 7.747789668545099317 ) ) ;
#7812=CARTESIAN_POINT ( 'NONE',  ( -8.497478458550677516, -21.44862750780143656, -1.500000000000002220 ) ) ;
#7815=CARTESIAN_POINT ( 'NONE',  ( -93.64041077057362372, -23.48783264082477018, -1.443836473390090580 ) ) ;
#7817=CARTESIAN_POINT ( 'NONE',  ( -121.5908097038916509, -23.96169478059713498, 10.65365249895717525 ) ) ;
#7818=CARTESIAN_POINT ( 'NONE',  ( -101.9507253916653440, -25.25287247409162816, 6.236250661346385726 ) ) ;
#7819=CARTESIAN_POINT ( 'NONE',  ( -111.5321115232925564, -25.10921514312168767, 3.478177734133227172 ) ) ;
#7820=CARTESIAN_POINT ( 'NONE',  ( -98.52287095715001897, -24.33832256527049154, 0.1851278514138618714 ) ) ;
#7821=CARTESIAN_POINT ( 'NONE',  ( -111.3157468039189695, -25.18425734897106594, 3.994351493279697518 ) ) ;
#7822=CARTESIAN_POINT ( 'NONE',  ( 3.219775368129482285, -19.64489633315863770, 11.49999999999998934 ) ) ;
#7824=CARTESIAN_POINT ( 'NONE',  ( -15.99800673754971037, 11.70972097625665675, -1.500000000000002220 ) ) ;
#7828=CARTESIAN_POINT ( 'NONE',  ( -109.6228709571500559, -29.50247984919015209, -1.443849546365048253 ) ) ;
#7829=CARTESIAN_POINT ( 'NONE',  ( 18.78520451414993531, -8.817701518030307994, 11.49999999999999645 ) ) ;
#7830=DIRECTION ( 'NONE',  ( -3.773278334453079618E-23, 0.9999999999976377785, 2.173523156925979975E-06 ) ) ;
#7831=B_SPLINE_CURVE_WITH_KNOTS ( 'NONE', 3,
 ( #63037, #93959, #24450, #86357 ),
 .UNSPECIFIED., .F., .F.,
 ( 4, 4 ),
 ( 0.6392306918040256969, 0.6402314388447910565 ),
 .UNSPECIFIED. ) ;
#7832=CARTESIAN_POINT ( 'NONE',  ( -106.6300389066096841, -23.96119346886880308, -0.6495511937832030291 ) ) ;
#7833=CARTESIAN_POINT ( 'NONE',  ( 17.68435195917723490, -14.24712819257710095, 11.49999999999999645 ) ) ;
#7834=ORIENTED_EDGE ( 'NONE', *, *, #64947, .F. ) ;
#7835=DIRECTION ( 'NONE',  ( -3.773278334453079030E-23, 0.9999999999976377785, 2.173523156925979128E-06 ) ) ;
#7836=B_SPLINE_CURVE_WITH_KNOTS ( 'NONE', 3,
 ( #45480, #46463, #46968, #6408 ),
 .UNSPECIFIED., .F., .F.,
 ( 4, 4 ),
 ( 0.000000000000000000, 9.999999999999592548E-05 ),
 .UNSPECIFIED. ) ;
#7838=VERTEX_POINT ( 'NONE', #31238 ) ;
#7840=CARTESIAN_POINT ( 'NONE',  ( -1.055277534996966970, 20.15608268182561247, -1.500000000000002220 ) ) ;
#7841=DIRECTION ( 'NONE',  ( 0.000000000000000000, 2.173523156925980399E-06, -0.9999999999976378895 ) ) ;
#7842=FACE_OUTER_BOUND ( 'NONE', #68154, .T. ) ;
#7843=ORIENTED_EDGE ( 'NONE', *, *, #44196, .T. ) ;
#7846=CARTESIAN_POINT ( 'NONE',  ( -16.32851894532483783, 16.03542138455653898, -1.500000000000002220 ) ) ;
#7847=CARTESIAN_POINT ( 'NONE',  ( -51.15490599271181082, -25.18439718008375650, 3.607700338875335699 ) ) ;
#7848=CARTESIAN_POINT ( 'NONE',  ( 10.18377579766961283, -19.05927572544859672, -1.500000000000002220 ) ) ;
#7852=CARTESIAN_POINT ( 'NONE',  ( 18.75483278694074940, -9.228467059531109129, 11.49999999999999645 ) ) ;
#7853=ORIENTED_EDGE ( 'NONE', *, *, #70527, .T. ) ;
#7854=CARTESIAN_POINT ( 'NONE',  ( -68.93918693012690824, -25.31612710229039109, 6.184868312322417516 ) ) ;
#7855=CARTESIAN_POINT ( 'NONE',  ( 4.628415685485613551, -21.52068878818806752, 11.49999999999998934 ) ) ;
#7860=DIRECTION ( 'NONE',  ( 0.000000000000000000, -2.173523156925980399E-06, 0.9999999999976378895 ) ) ;
#7863=CARTESIAN_POINT ( 'NONE',  ( -72.50260992981964137, -24.35071581493542681, 9.817618358456032368 ) ) ;
#7866=CARTESIAN_POINT ( 'NONE',  ( -71.50674337012141280, -24.15620529776628445, 10.23563542870660115 ) ) ;
#7868=CARTESIAN_POINT ( 'NONE',  ( -36.53864600885722780, -24.34968618360933235, 0.1864209137778783110 ) ) ;
#7869=EDGE_CURVE ( 'NONE', #43640, #76269, #98180, .T. ) ;
#7870=CARTESIAN_POINT ( 'NONE',  ( 20.35601985306173134, -1.938729116259007679, -1.500000000000002220 ) ) ;
#7871=EDGE_LOOP ( 'NONE', ( #2626, #71266, #92908, #4929 ) ) ;
#7872=CARTESIAN_POINT ( 'NONE',  ( -110.6228709571500559, -24.99156045073393173, 7.747789690856161648 ) ) ;
#7874=LINE ( 'NONE', #78374, #19145 ) ;
#7875=CARTESIAN_POINT ( 'NONE',  ( -18.06118310651259407, 13.05043149098080058, 11.49999999999998934 ) ) ;
#7878=EDGE_LOOP ( 'NONE', ( #69927, #26381, #25146, #38208 ) ) ;
#7880=CARTESIAN_POINT ( 'NONE',  ( -29.01900995608618317, -24.63645947259608704, 7.711474408511321599 ) ) ;
#7881=CARTESIAN_POINT ( 'NONE',  ( -5.744250498300313090, 20.02623800365557472, 11.49999999999998934 ) ) ;
#7882=ORIENTED_EDGE ( 'NONE', *, *, #83132, .T. ) ;
#7884=ORIENTED_EDGE ( 'NONE', *, *, #85072, .T. ) ;
#7885=B_SPLINE_SURFACE_WITH_KNOTS ( 'NONE', 3, 3, ( 
 ( #25171, #11452, #10448, #96199 ),
 ( #88089, #56146, #50033, #80968 ),
 ( #71865, #42430, #3858, #2354 ),
 ( #33283, #33793, #79961, #64271 ),
 ( #51024, #6333, #76327, #4842 ),
 ( #6826, #28181, #27685, #35795 ),
 ( #37290, #82457, #36791, #58634 ) ),
 .UNSPECIFIED., .F., .F., .F.,
 ( 4, 3, 4 ),
 ( 4, 4 ),
 ( 0.0004766839783834107900, 0.1029713700210899974, 0.2054660560637965871 ),
 ( 0.8797177824225477227, 0.8811364071469682813 ),
 .UNSPECIFIED. ) ;
#7887=CARTESIAN_POINT ( 'NONE',  ( -14.15979099334852798, -15.53166555317341135, -1.500000000000002220 ) ) ;
#7894=CARTESIAN_POINT ( 'NONE',  ( -92.51514722113715550, -23.96169478059712787, 10.65365249895717525 ) ) ;
#7895=FACE_OUTER_BOUND ( 'NONE', #37736, .T. ) ;
#7896=CARTESIAN_POINT ( 'NONE',  ( -5.848988146064017180, 21.40304369876291446, 11.49999999999999645 ) ) ;
#7897=ORIENTED_EDGE ( 'NONE', *, *, #62600, .T. ) ;
#7898=CARTESIAN_POINT ( 'NONE',  ( -98.92109765663163046, -25.28792679843457236, 5.825529105375064631 ) ) ;
#7899=LINE ( 'NONE', #38851, #92662 ) ;
#7900=VERTEX_POINT ( 'NONE', #84524 ) ;
#7901=CARTESIAN_POINT ( 'NONE',  ( 21.71957326813621592, -6.446789169762093152, 11.49999999999998934 ) ) ;
#7902=VECTOR ( 'NONE', #78823, 1000.000000000000114 ) ;
#7905=EDGE_CURVE ( 'NONE', #52694, #21736, #57055, .T. ) ;
#7910=B_SPLINE_CURVE_WITH_KNOTS ( 'NONE', 3,
 ( #38715, #92499, #52458, #48224 ),
 .UNSPECIFIED., .F., .F.,
 ( 4, 4 ),
 ( 0.000000000000000000, 9.999999999998206125E-05 ),
 .UNSPECIFIED. ) ;
#7911=B_SPLINE_CURVE_WITH_KNOTS ( 'NONE', 3,
 ( #75605, #6613, #99938, #15720, #68027, #52796, #8119, #39061, #68516, #38565 ),
 .UNSPECIFIED., .F., .F.,
 ( 4, 2, 2, 2, 4 ),
 ( 1.734723475976807094E-18, 0.0001825288931172122913, 0.0003650577862344228479, 0.0005475866793516334045, 0.0007301155724688439611 ),
 .UNSPECIFIED. ) ;
#7912=CARTESIAN_POINT ( 'NONE',  ( -4.233023369943174075, 19.68221892606961987, -1.500000000000002220 ) ) ;
#7916=CARTESIAN_POINT ( 'NONE',  ( -9.622923231576368863, -20.19340101508991125, -1.500000000000002220 ) ) ;
#7918=ORIENTED_EDGE ( 'NONE', *, *, #89295, .F. ) ;
#7920=CARTESIAN_POINT ( 'NONE',  ( -94.62560501205011576, -24.51419770103156281, 9.386484678747184063 ) ) ;
#7921=CARTESIAN_POINT ( 'NONE',  ( -85.52287095715006160, -23.47596703998600631, 11.44779298504228393 ) ) ;
#7923=CARTESIAN_POINT ( 'NONE',  ( -97.25306485665333867, -24.26743686635980879, 0.04347934593174130474 ) ) ;
#7924=CARTESIAN_POINT ( 'NONE',  ( 18.00893756148942870, 7.586210683597776949, 11.49999999999998934 ) ) ;
#7925=CARTESIAN_POINT ( 'NONE',  ( -102.5228709571500758, -24.65952944569305316, 1.056160979905702346 ) ) ;
#7926=CARTESIAN_POINT ( 'NONE',  ( 18.54456287915894563, -10.88813254144886322, -1.500000000000002220 ) ) ;
#7927=CARTESIAN_POINT ( 'NONE',  ( -36.52287095715006160, -24.34917612406836795, 0.1852690917426497719 ) ) ;
#7931=CARTESIAN_POINT ( 'NONE',  ( -11.09240565882118368, -20.00103931635436538, -1.500000000000002220 ) ) ;
#7934=DIRECTION ( 'NONE',  ( 0.000000000000000000, 0.9999999999976377785, 2.173523156925979128E-06 ) ) ;
#7936=CARTESIAN_POINT ( 'NONE',  ( -10.42242239376218116, -17.14354752861867937, 11.49999999999999645 ) ) ;
#7938=PLANE ( 'NONE',  #79203 ) ;
#7940=CARTESIAN_POINT ( 'NONE',  ( -103.6228709571500559, -24.64898659630368627, 1.056161002820829697 ) ) ;
#7942=PLANE ( 'NONE',  #21851 ) ;
#7943=CARTESIAN_POINT ( 'NONE',  ( -92.62287095715008434, -24.51283580621364067, 0.6167428607019841413 ) ) ;
#7944=CARTESIAN_POINT ( 'NONE',  ( -3.653784360050144286, 21.42803128968991544, -1.500000000000002220 ) ) ;
#7946=CARTESIAN_POINT ( 'NONE',  ( -106.6228709571500559, -24.64965695001469115, 8.947790433994176951 ) ) ;
#7947=CARTESIAN_POINT ( 'NONE',  ( -17.63651738508609412, 8.604534254076446231, -1.500000000000002220 ) ) ;
#7948=CARTESIAN_POINT ( 'NONE',  ( -38.55620429048340725, -23.48786465467240347, 11.44779295918255180 ) ) ;
#7949=CARTESIAN_POINT ( 'NONE',  ( -104.5562042904833930, -23.48786465467241769, 11.44779295918253759 ) ) ;
#7951=CARTESIAN_POINT ( 'NONE',  ( -91.50656180577668408, -24.51419770103159124, 9.386484678747176957 ) ) ;
#7953=CARTESIAN_POINT ( 'NONE',  ( -6.273408026305254737, 19.60348359158234288, 11.49999999999999645 ) ) ;
#7955=CARTESIAN_POINT ( 'NONE',  ( -47.62287095715004881, -23.48783264082478084, -1.443836473390070596 ) ) ;
#7957=CARTESIAN_POINT ( 'NONE',  ( -70.32380231474228083, -25.12219144746705268, 7.101635560771297762 ) ) ;
#7958=CARTESIAN_POINT ( 'NONE',  ( -39.89668141102733756, -25.18430903175396907, 3.440461233786359596 ) ) ;
#7960=CARTESIAN_POINT ( 'NONE',  ( -74.52287095715003318, -23.95044443724992078, 10.65354141964648882 ) ) ;
#7961=CARTESIAN_POINT ( 'NONE',  ( -69.52287095715006160, -24.64965694238407323, 8.947790433994200043 ) ) ;
#7964=CARTESIAN_POINT ( 'NONE',  ( -25.56960729154874556, -24.93063093467123181, 5.760627416161578473 ) ) ;
#7965=FACE_OUTER_BOUND ( 'NONE', #33857, .T. ) ;
#7967=CARTESIAN_POINT ( 'NONE',  ( -14.58522200957802184, -17.87834940746265389, 11.49999999999999645 ) ) ;
#7968=CARTESIAN_POINT ( 'NONE',  ( 22.53581206741051446, 3.480912172000575122, -1.500000000000002220 ) ) ;
#7969=CARTESIAN_POINT ( 'NONE',  ( -74.51178750762115044, -23.96119346886879953, -0.6495511937832119109 ) ) ;
#7970=AXIS2_PLACEMENT_3D ( 'NONE', #30556, #53911, #5726 ) ;
#7971=CARTESIAN_POINT ( 'NONE',  ( -105.6228709571500701, -24.82558206586147875, 1.605769216559634005 ) ) ;
#7972=CARTESIAN_POINT ( 'NONE',  ( -57.52287095715006160, -24.33832256527049154, 0.1851278514138604558 ) ) ;
#7973=CARTESIAN_POINT ( 'NONE',  ( 22.28251467978060063, -2.329348454117679879, 11.49999999999999645 ) ) ;
#7976=CARTESIAN_POINT ( 'NONE',  ( -69.52287095715006160, -24.65952944569304606, 1.056160979905697239 ) ) ;
#7978=CARTESIAN_POINT ( 'NONE',  ( -9.563806973793814947, 19.74097577964120376, -1.500000000000002220 ) ) ;
#7979=EDGE_CURVE ( 'NONE', #28755, #59566, #29174, .T. ) ;
#7980=CARTESIAN_POINT ( 'NONE',  ( -54.55620429048339304, -23.48783264082478084, -1.443836473390070596 ) ) ;
#7981=CARTESIAN_POINT ( 'NONE',  ( -87.64317292477575450, -23.48786465467240703, 11.44779295918254647 ) ) ;
#7982=CARTESIAN_POINT ( 'NONE',  ( -121.5228709571500332, -24.50321055353803246, 9.387540953477520489 ) ) ;
#7983=B_SPLINE_CURVE_WITH_KNOTS ( 'NONE', 3,
 ( #2080, #93396, #25397, #95413, #80189, #55870 ),
 .UNSPECIFIED., .F., .F.,
 ( 4, 2, 4 ),
 ( 0.000000000000000000, 0.001380764517854766484, 0.002761529035709532967 ),
 .UNSPECIFIED. ) ;
#7984=CARTESIAN_POINT ( 'NONE',  ( -78.50859902716933902, -24.15543982623907127, -0.2315651400026641771 ) ) ;
#7985=LINE ( 'NONE', #24209, #12827 ) ;
#7986=ORIENTED_EDGE ( 'NONE', *, *, #39138, .T. ) ;
#7987=CARTESIAN_POINT ( 'NONE',  ( -18.14515864413662172, 9.488524743509296755, -1.500000000000002220 ) ) ;
#7988=ORIENTED_EDGE ( 'NONE', *, *, #5593, .F. ) ;
#7990=ORIENTED_EDGE ( 'NONE', *, *, #49574, .F. ) ;
#7991=VERTEX_POINT ( 'NONE', #77399 ) ;
#7992=CARTESIAN_POINT ( 'NONE',  ( 16.10802587768190008, -16.50329280669357246, -1.500000000000002220 ) ) ;
#7994=EDGE_CURVE ( 'NONE', #41799, #76858, #7899, .T. ) ;
#7995=CARTESIAN_POINT ( 'NONE',  ( 11.01437679584920026, 17.03896688766576517, -1.500000000000002220 ) ) ;
#7997=FACE_OUTER_BOUND ( 'NONE', #53383, .T. ) ;
#7998=CARTESIAN_POINT ( 'NONE',  ( -72.52287095715007581, -23.94994826722564696, -0.6494450866342730277 ) ) ;
#7999=EDGE_CURVE ( 'NONE', #88644, #90885, #9961, .T. ) ;
#8001=CARTESIAN_POINT ( 'NONE',  ( -70.65050961511018102, -23.85016227208580730, -0.8807180028928335291 ) ) ;
#8002=CARTESIAN_POINT ( 'NONE',  ( -17.55493245422511350, -12.44833567967518029, 11.49999999999999645 ) ) ;
#8003=EDGE_LOOP ( 'NONE', ( #98106, #47085, #32484, #80010, #85909, #68219, #65466, #15153 ) ) ;
#8004=CARTESIAN_POINT ( 'NONE',  ( -80.62287095715005592, -29.50248789122583659, 2.256150453626215580 ) ) ;
#8005=CARTESIAN_POINT ( 'NONE',  ( -61.64838989061559005, -23.73791477778911840, 11.05961554403170943 ) ) ;
#8006=ORIENTED_EDGE ( 'NONE', *, *, #59194, .F. ) ;
#8007=CARTESIAN_POINT ( 'NONE',  ( 17.22178217532253086, -11.58000449095910867, -1.500000000000002220 ) ) ;
#8008=ORIENTED_EDGE ( 'NONE', *, *, #74075, .F. ) ;
#8011=ORIENTED_EDGE ( 'NONE', *, *, #25631, .T. ) ;
#8013=FACE_OUTER_BOUND ( 'NONE', #21134, .T. ) ;
#8015=ORIENTED_EDGE ( 'NONE', *, *, #17334, .T. ) ;
#8017=CARTESIAN_POINT ( 'NONE',  ( -42.50578598728685620, -23.96169478059712787, 10.65365249895718947 ) ) ;
#8018=CARTESIAN_POINT ( 'NONE',  ( -65.48565870665615307, -24.92564183028979130, 1.928384488918254869 ) ) ;
#8019=CARTESIAN_POINT ( 'NONE',  ( 17.26801960494244881, -13.64313956103151071, 11.49999999999999645 ) ) ;
#8021=CARTESIAN_POINT ( 'NONE',  ( 1.861690257272737847, 22.46465895387273903, -1.500000000000002220 ) ) ;
#8022=CARTESIAN_POINT ( 'NONE',  ( 8.398332666215036824, -19.25654272332048578, 11.49999999999998934 ) ) ;
#8024=ORIENTED_EDGE ( 'NONE', *, *, #31197, .T. ) ;
#8025=ORIENTED_EDGE ( 'NONE', *, *, #18839, .F. ) ;
#8026=CARTESIAN_POINT ( 'NONE',  ( -36.62287095715006302, -24.65952944569303895, 1.056160979905693909 ) ) ;
#8028=CARTESIAN_POINT ( 'NONE',  ( -17.63906703526961550, 12.34593017946836291, -1.500000000000002220 ) ) ;
#8029=EDGE_CURVE ( 'NONE', #40387, #89148, #40360, .T. ) ;
#8030=CARTESIAN_POINT ( 'NONE',  ( -73.52287095715007581, -29.50248528299804818, 1.056150453629036701 ) ) ;
#8031=ORIENTED_EDGE ( 'NONE', *, *, #43351, .F. ) ;
#8032=CARTESIAN_POINT ( 'NONE',  ( 14.48694714638828884, 15.39972936300609341, 11.49999999999998934 ) ) ;
#8033=CARTESIAN_POINT ( 'NONE',  ( -83.52287095715006160, -24.64898659630367916, 1.056161002820826145 ) ) ;
#8034=CARTESIAN_POINT ( 'NONE',  ( -51.20402663469029392, -25.03148705966398069, 7.397224223744971461 ) ) ;
#8036=CARTESIAN_POINT ( 'NONE',  ( -121.6275741054623722, -23.48783264082477018, -1.443836473390087694 ) ) ;
#8037=DIRECTION ( 'NONE',  ( -3.773278334453079618E-23, 0.9999999999976377785, 2.173523156925979975E-06 ) ) ;
#8039=CARTESIAN_POINT ( 'NONE',  ( -15.97456084408017674, 15.39233244482803009, -1.500000000000002220 ) ) ;
#8040=CARTESIAN_POINT ( 'NONE',  ( -81.64116179052845723, -23.73791477778912196, 11.05961554403170943 ) ) ;
#8042=CARTESIAN_POINT ( 'NONE',  ( -51.26059310326842677, -25.31633111157479021, 5.062965957937453965 ) ) ;
#8043=DIRECTION ( 'NONE',  ( -4.522247983293619802E-39, -2.173523156893721996E-06, 0.9999999999976377785 ) ) ;
#8045=VECTOR ( 'NONE', #82900, 1000.000000000000114 ) ;
#8046=B_SPLINE_CURVE_WITH_KNOTS ( 'NONE', 3,
 ( #31452, #37568, #68520, #99451, #49205, #1518 ),
 .UNSPECIFIED., .F., .F.,
 ( 4, 2, 4 ),
 ( 0.000000000000000000, 0.001380764517853252937, 0.002761529035706505875 ),
 .UNSPECIFIED. ) ;
#8049=VECTOR ( 'NONE', #25464, 1000.000000000000114 ) ;
#8050=CARTESIAN_POINT ( 'NONE',  ( 18.36381783059253081, 6.383776564742674964, 11.49999999999998934 ) ) ;
#8051=VECTOR ( 'NONE', #98572, 1000.000000000000114 ) ;
#8052=CARTESIAN_POINT ( 'NONE',  ( -8.434714792116727367, -19.68496499552307455, 11.49999999999998934 ) ) ;
#8054=CARTESIAN_POINT ( 'NONE',  ( -60.55976160235340444, -23.85049219812968957, 10.88485053497088728 ) ) ;
#8056=CARTESIAN_POINT ( 'NONE',  ( -101.1965263674405691, -25.18440091922403568, 3.665446597890811731 ) ) ;
#8057=CARTESIAN_POINT ( 'NONE',  ( 9.518656604726816184, -20.62229310799655124, -1.500000000000002220 ) ) ;
#8058=EDGE_CURVE ( 'NONE', #28096, #79008, #11409, .T. ) ;
#8060=EDGE_CURVE ( 'NONE', #28964, #71576, #3865, .T. ) ;
#8061=CARTESIAN_POINT ( 'NONE',  ( -41.52287095715006870, -29.50248528299804818, 1.056150453629031594 ) ) ;
#8062=CARTESIAN_POINT ( 'NONE',  ( -127.6228709571500843, -23.73907113216990794, -1.053371485793217932 ) ) ;
#8063=CARTESIAN_POINT ( 'NONE',  ( 13.50462702941046977, 14.53317887778067252, 11.49999999999999645 ) ) ;
#8066=EDGE_LOOP ( 'NONE', ( #52467, #74425, #15345, #80773 ) ) ;
#8067=CARTESIAN_POINT ( 'NONE',  ( -45.62287095715006302, -24.62226745350437795, 0.9660975649728075210 ) ) ;
#8070=CARTESIAN_POINT ( 'NONE',  ( 5.966611984012316405, 20.80180421262142687, 11.49999999999998934 ) ) ;
#8072=CARTESIAN_POINT ( 'NONE',  ( -56.53341610917590287, -24.66019654487199375, 8.947790411086122830 ) ) ;
#8073=CARTESIAN_POINT ( 'NONE',  ( 12.19879910451502703, -15.15100395215988449, -1.500000000000002220 ) ) ;
#8075=CARTESIAN_POINT ( 'NONE',  ( -55.48263523968800115, -24.83644354573578283, 8.397322867130096569 ) ) ;
#8076=CARTESIAN_POINT ( 'NONE',  ( -0.3680779360730609406, 19.82951397037014729, 11.49999999999998934 ) ) ;
#8079=CARTESIAN_POINT ( 'NONE',  ( -5.191926799570463658, 19.71030214607805675, 11.49999999999999645 ) ) ;
#8080=CARTESIAN_POINT ( 'NONE',  ( -80.49781194617861502, -24.73486907724918282, 1.287355809206963908 ) ) ;
#8081=LINE ( 'NONE', #972, #414 ) ;
#8082=B_SPLINE_CURVE_WITH_KNOTS ( 'NONE', 3,
 ( #13331, #90472, #97581, #90965 ),
 .UNSPECIFIED., .F., .F.,
 ( 4, 4 ),
 ( 0.000000000000000000, 9.999999999997510880E-05 ),
 .UNSPECIFIED. ) ;
#8084=B_SPLINE_SURFACE_WITH_KNOTS ( 'NONE', 3, 3, ( 
 ( #86587, #78965, #23170, #24678 ),
 ( #15074, #48039, #84584, #46042 ),
 ( #8964, #39419, #23677, #85085 ),
 ( #24184, #93694, #61770, #93192 ),
 ( #70368, #17074, #76963, #15570 ),
 ( #55160, #16566, #92689, #85584 ),
 ( #855, #37919, #7456, #39913 ),
 ( #38413, #32302, #16067, #68867 ),
 ( #47040, #99787, #69366, #30295 ),
 ( #61274, #92195, #77955, #22672 ) ),
 .UNSPECIFIED., .F., .F., .F.,
 ( 4, 3, 3, 4 ),
 ( 4, 4 ),
 ( 0.7022005934544808259, 0.7765311282028795059, 0.8508616629512780749, 0.9995227324480753239 ),
 ( 0.04949997043182981921, 0.05054219703631999960 ),
 .UNSPECIFIED. ) ;
#8086=DIRECTION ( 'NONE',  ( 1.000000000000000000, 3.773278334444166432E-23, 8.201307841325785021E-29 ) ) ;
#8087=CARTESIAN_POINT ( 'NONE',  ( -49.53270844027763786, -25.31601842583603457, 5.057855796360450462 ) ) ;
#8088=CARTESIAN_POINT ( 'NONE',  ( -128.6228709571500417, -24.34917612406839993, 0.1852690917426724204 ) ) ;
#8090=CARTESIAN_POINT ( 'NONE',  ( 12.55954966114946458, -15.69740789531843461, 11.49999999999998934 ) ) ;
#8091=B_SPLINE_CURVE_WITH_KNOTS ( 'NONE', 3,
 ( #100038, #99544, #28555, #68622, #45293, #30043 ),
 .UNSPECIFIED., .F., .F.,
 ( 4, 2, 4 ),
 ( 1.570887131794952276E-05, 0.001396322306279765193, 0.002776935741241580609 ),
 .UNSPECIFIED. ) ;
#8092=EDGE_CURVE ( 'NONE', #59704, #59375, #76429, .T. ) ;
#8093=DIRECTION ( 'NONE',  ( -3.773278334453079030E-23, 0.9999999999976377785, 2.173523156925979128E-06 ) ) ;
#8094=ORIENTED_EDGE ( 'NONE', *, *, #12125, .T. ) ;
#8096=CARTESIAN_POINT ( 'NONE',  ( 16.30191990219073972, -16.09819076282585826, 11.49999999999999645 ) ) ;
#8097=CARTESIAN_POINT ( 'NONE',  ( -17.38503614929206265, -14.63273120789127013, -1.500000000000002220 ) ) ;
#8100=DIRECTION ( 'NONE',  ( 0.000000000000000000, -2.173523156925980399E-06, 0.9999999999976378895 ) ) ;
#8101=CARTESIAN_POINT ( 'NONE',  ( -39.58729228046302495, -25.24755811718921095, 3.712701613397900058 ) ) ;
#8102=LINE ( 'NONE', #85223, #93441 ) ;
#8107=EDGE_CURVE ( 'NONE', #89671, #82714, #94592, .T. ) ;
#8111=CARTESIAN_POINT ( 'NONE',  ( 2.554409723529738052, 20.22502395925995700, 11.49999999999998934 ) ) ;
#8113=B_SPLINE_CURVE_WITH_KNOTS ( 'NONE', 3,
 ( #22651, #17429, #2223, #25545 ),
 .UNSPECIFIED., .F., .F.,
 ( 4, 4 ),
 ( 0.000000000000000000, 9.999999999998897304E-05 ),
 .UNSPECIFIED. ) ;
#8114=CARTESIAN_POINT ( 'NONE',  ( -15.63304604236160067, -16.83380969201049382, 11.49999999999998934 ) ) ;
#8116=CARTESIAN_POINT ( 'NONE',  ( -103.5895376238167245, -23.48783264082478794, -1.443836473390062158 ) ) ;
#8117=EDGE_LOOP ( 'NONE', ( #70903, #7142, #71057, #50188, #82681, #26718, #75362, #32837, #42674, #43108, #29124, #73513, #62446, #58751, #13255, #60915, #8387, #75511, #73530, #31749 ) ) ;
#8119=CARTESIAN_POINT ( 'NONE',  ( -101.3556973279126368, -25.18955741793521597, 6.678808583419815648 ) ) ;
#8120=EDGE_CURVE ( 'NONE', #7991, #78336, #79199, .T. ) ;
#8121=CARTESIAN_POINT ( 'NONE',  ( -80.71993455722410715, -25.13732816275518900, 7.077603319917434632 ) ) ;
#8122=ADVANCED_FACE ( 'NONE', ( #80918 ), #48484, .F. ) ;
#8124=CARTESIAN_POINT ( 'NONE',  ( -111.5228709571500616, -24.33927499327855770, 9.819080762295804732 ) ) ;
#8125=CARTESIAN_POINT ( 'NONE',  ( 18.88549913130557556, 9.949676122998861061, 11.49999999999999645 ) ) ;
#8126=VERTEX_POINT ( 'NONE', #52471 ) ;
#8127=AXIS2_PLACEMENT_3D ( 'NONE', #37183, #66668, #75238 ) ;
#8128=ORIENTED_EDGE ( 'NONE', *, *, #17465, .T. ) ;
#8129=CARTESIAN_POINT ( 'NONE',  ( 22.20243239366838850, -0.07139729354238147363, -1.500000000000002220 ) ) ;
#8130=B_SPLINE_CURVE_WITH_KNOTS ( 'NONE', 3,
 ( #79575, #85185, #20165, #66865, #87694, #80573 ),
 .UNSPECIFIED., .F., .F.,
 ( 4, 2, 4 ),
 ( 6.384118678611318703E-06, 0.001386860460828374551, 0.002767336802978137555 ),
 .UNSPECIFIED. ) ;
#8131=CARTESIAN_POINT ( 'NONE',  ( 17.37421522561336928, 11.14841987994331696, -1.500000000000002220 ) ) ;
#8135=CARTESIAN_POINT ( 'NONE',  ( -109.3320997930167806, -25.27682792883151919, 5.169840796200587008 ) ) ;
#8136=EDGE_CURVE ( 'NONE', #18610, #20866, #86385, .T. ) ;
#8137=CARTESIAN_POINT ( 'NONE',  ( -71.72827525033231666, -25.11539253604531297, 2.804427796191110378 ) ) ;
#8139=CARTESIAN_POINT ( 'NONE',  ( -49.52581182275615390, -25.18689758514837251, 6.769651850996265985 ) ) ;
#8140=ORIENTED_EDGE ( 'NONE', *, *, #36921, .T. ) ;
#8141=CARTESIAN_POINT ( 'NONE',  ( -56.58953762381672448, -24.64965694238407323, 8.947790433994656567 ) ) ;
#8143=CARTESIAN_POINT ( 'NONE',  ( 5.792680761630559338, -19.98616098212858105, -1.500000000000002220 ) ) ;
#8144=CARTESIAN_POINT ( 'NONE',  ( -3.523925741820590929, 21.50064390955241578, 11.49999999999999645 ) ) ;
#8145=DIRECTION ( 'NONE',  ( -3.773278334444166432E-23, 1.000000000000000000, 0.000000000000000000 ) ) ;
#8146=CARTESIAN_POINT ( 'NONE',  ( -100.3501680573226906, -25.03346342031885641, 7.560302575324243435 ) ) ;
#8147=CARTESIAN_POINT ( 'NONE',  ( -11.43049785330379997, -19.34545768653811493, 11.49999999999998934 ) ) ;
#8148=CARTESIAN_POINT ( 'NONE',  ( -34.52287095715006160, -24.64898659630366851, 1.056161002820817485 ) ) ;
#8150=CARTESIAN_POINT ( 'NONE',  ( -109.6228709571500559, -29.50250786944525672, 11.44777988621622988 ) ) ;
#8152=ORIENTED_EDGE ( 'NONE', *, *, #23929, .F. ) ;
#8155=CARTESIAN_POINT ( 'NONE',  ( 19.36035776617087123, -9.008237321879198234, -1.500000000000002220 ) ) ;
#8156=ORIENTED_EDGE ( 'NONE', *, *, #45300, .T. ) ;
#8157=CARTESIAN_POINT ( 'NONE',  ( -19.04630365209304799, -9.011775662611203330, 11.49999999999998934 ) ) ;
#8158=CARTESIAN_POINT ( 'NONE',  ( -30.47189565061154326, -23.47430189329197248, -1.443836490256471983 ) ) ;
#8159=CARTESIAN_POINT ( 'NONE',  ( 16.79105032741591330, -10.77411451815220822, -1.500000000000002220 ) ) ;
#8162=CARTESIAN_POINT ( 'NONE',  ( -8.471812324360341151, -20.26817064352238162, -1.500000000000002220 ) ) ;
#8163=FACE_OUTER_BOUND ( 'NONE', #95226, .T. ) ;
#8165=CARTESIAN_POINT ( 'NONE',  ( -65.57704458058132957, -25.00182538069147142, 7.747789668545043362 ) ) ;
#8167=CARTESIAN_POINT ( 'NONE',  ( -6.911038104174170194, -19.68591361114308214, 11.49999999999999645 ) ) ;
#8169=CARTESIAN_POINT ( 'NONE',  ( -125.5228709571500900, -24.91570333825475458, 8.075032458260897883 ) ) ;
#8171=CARTESIAN_POINT ( 'NONE',  ( -30.60531187098371575, -24.66542028447632262, 8.909134979017295564 ) ) ;
#8172=CARTESIAN_POINT ( 'NONE',  ( 19.49461108348020133, 8.573440864381753457, 11.49999999999998934 ) ) ;
#8174=CARTESIAN_POINT ( 'NONE',  ( -107.6262921065285241, -24.35071581493543746, 9.817618358456021710 ) ) ;
#8178=CARTESIAN_POINT ( 'NONE',  ( -15.68175098440391402, -16.16561365185589594, -1.500000000000002220 ) ) ;
#8180=CARTESIAN_POINT ( 'NONE',  ( -129.5895376238167387, -24.66019654487200086, 8.947790411086117501 ) ) ;
#8181=ORIENTED_EDGE ( 'NONE', *, *, #91785, .T. ) ;
#8182=EDGE_CURVE ( 'NONE', #47263, #58944, #89529, .T. ) ;
#8183=CARTESIAN_POINT ( 'NONE',  ( -104.5228709571500758, -23.48786465467241769, 11.44779295918254114 ) ) ;
#8184=CARTESIAN_POINT ( 'NONE',  ( 19.16472379399037251, -4.548241762842377689, 11.49999999999999645 ) ) ;
#8185=CARTESIAN_POINT ( 'NONE',  ( -125.6228709571500559, -24.63287334234178161, 0.9662140553045557301 ) ) ;
#8188=EDGE_CURVE ( 'NONE', #44155, #96177, #54944, .T. ) ;
#8191=CARTESIAN_POINT ( 'NONE',  ( -89.90116859791649517, -25.30572777988223976, 5.920366768842380445 ) ) ;
#8192=ADVANCED_FACE ( 'NONE', ( #28136 ), #3811, .F. ) ;
#8194=FACE_OUTER_BOUND ( 'NONE', #93674, .T. ) ;
#8195=CARTESIAN_POINT ( 'NONE',  ( 12.09797951242163805, 15.59582292391970704, 11.49999999999998934 ) ) ;
#8196=ORIENTED_EDGE ( 'NONE', *, *, #55698, .F. ) ;
#8198=ADVANCED_FACE ( 'NONE', ( #42872 ), #90522, .T. ) ;
#8199=CARTESIAN_POINT ( 'NONE',  ( -109.3903331153901206, -25.27100251396372244, 3.960067624998357960 ) ) ;
#8202=ORIENTED_EDGE ( 'NONE', *, *, #21124, .T. ) ;
#8203=CARTESIAN_POINT ( 'NONE',  ( -81.42380231474228935, -29.50249428492551829, 5.197779886230994073 ) ) ;
#8204=CARTESIAN_POINT ( 'NONE',  ( -89.62287095715004170, -29.50248528299804818, 1.056150453629040253 ) ) ;
#8205=CARTESIAN_POINT ( 'NONE',  ( -69.56655373305933665, -25.28935879948601695, 5.635482696873745923 ) ) ;
#8207=DIRECTION ( 'NONE',  ( 1.000000000000000000, 3.773278334444167608E-23, 8.201307810031787050E-29 ) ) ;
#8209=CARTESIAN_POINT ( 'NONE',  ( -94.58953762381672448, -24.65952944569304961, 1.056160979905703678 ) ) ;
#8210=CARTESIAN_POINT ( 'NONE',  ( -43.62287095715004170, -23.48786465467241058, 11.44779295918255180 ) ) ;
#8211=CARTESIAN_POINT ( 'NONE',  ( -18.81269933604069067, 6.858547123926768130, -1.500000000000002220 ) ) ;
#8212=EDGE_CURVE ( 'NONE', #42958, #11783, #50106, .T. ) ;
#8213=CARTESIAN_POINT ( 'NONE',  ( -100.0924861708260636, -25.10935045777317498, 2.869718873696385675 ) ) ;
#8214=PLANE ( 'NONE',  #43554 ) ;
#8217=CARTESIAN_POINT ( 'NONE',  ( -79.55429133993682456, -23.96169478059713143, 10.65365249895718058 ) ) ;
#8218=CARTESIAN_POINT ( 'NONE',  ( -110.2348554541972874, -25.18430154389852049, 3.296590759564009154 ) ) ;
#8219=CARTESIAN_POINT ( 'NONE',  ( -35.54983106724529307, -24.15503026093914940, -0.2815557561904327155 ) ) ;
#8220=CARTESIAN_POINT ( 'NONE',  ( -39.56136241089613748, -25.30385213834873781, 5.536731319770037629 ) ) ;
#8221=B_SPLINE_CURVE_WITH_KNOTS ( 'NONE', 3,
 ( #5447, #60749, #36898, #91671 ),
 .UNSPECIFIED., .F., .F.,
 ( 4, 4 ),
 ( 0.1298786676550697794, 0.1388850989271851466 ),
 .UNSPECIFIED. ) ;
#8222=FACE_OUTER_BOUND ( 'NONE', #71721, .T. ) ;
#8226=CARTESIAN_POINT ( 'NONE',  ( -40.52287095715006160, -24.62285846331440098, 9.038163153548140372 ) ) ;
#8228=CARTESIAN_POINT ( 'NONE',  ( 20.23688964843749005, 1.552196809742036221, -1.500000000000002220 ) ) ;
#8229=DIRECTION ( 'NONE',  ( -0.8254963646400337307, 1.226752628532750849E-06, -0.5644074343633185276 ) ) ;
#8230=CARTESIAN_POINT ( 'NONE',  ( -99.62287095715001328, -24.33832256526968862, 0.1851278514119927554 ) ) ;
#8232=VERTEX_POINT ( 'NONE', #43861 ) ;
#8234=CARTESIAN_POINT ( 'NONE',  ( 17.77915467781788195, 9.360003092772107181, -1.500000000000002220 ) ) ;
#8235=CARTESIAN_POINT ( 'NONE',  ( -13.19772682967519195, -16.48504770976277101, 11.49999999999999645 ) ) ;
#8236=CARTESIAN_POINT ( 'NONE',  ( 21.87352179494074633, -3.179377960941109915, -1.500000000000002220 ) ) ;
#8237=VECTOR ( 'NONE', #58203, 1000.000000000000114 ) ;
#8238=EDGE_CURVE ( 'NONE', #2872, #95000, #91019, .T. ) ;
#8239=CARTESIAN_POINT ( 'NONE',  ( 11.66944253441096002, 16.90307425063352298, -1.500000000000002220 ) ) ;
#8240=CARTESIAN_POINT ( 'NONE',  ( -60.58607451518173548, -24.63355581998385446, 0.9682620441943891043 ) ) ;
#8241=ORIENTED_EDGE ( 'NONE', *, *, #31626, .F. ) ;
#8244=CARTESIAN_POINT ( 'NONE',  ( -88.52287095715006160, -24.64965694238407323, 8.947790433994196491 ) ) ;
#8245=CARTESIAN_POINT ( 'NONE',  ( -70.52287095715009002, -24.82576562948882781, 8.398263436605597931 ) ) ;
#8246=ORIENTED_EDGE ( 'NONE', *, *, #10282, .F. ) ;
#8249=DIRECTION ( 'NONE',  ( 0.000000000000000000, -0.9999999999976377785, -2.173523156925979128E-06 ) ) ;
#8250=CARTESIAN_POINT ( 'NONE',  ( -49.41210582477036439, -25.09381984642397612, 7.261948667840803395 ) ) ;
#8252=CARTESIAN_POINT ( 'NONE',  ( -3.087264924507187924, 20.40197043678811539, -1.500000000000002220 ) ) ;
#8254=CARTESIAN_POINT ( 'NONE',  ( 10.18377579766961283, -19.05927572544859672, 11.49999999999999645 ) ) ;
#8255=ORIENTED_EDGE ( 'NONE', *, *, #8996, .T. ) ;
#8256=FACE_OUTER_BOUND ( 'NONE', #4281, .T. ) ;
#8258=CARTESIAN_POINT ( 'NONE',  ( 6.497064355747536268, 21.42967291005575348, -1.500000000000002220 ) ) ;
#8259=CARTESIAN_POINT ( 'NONE',  ( -67.22287095715007865, -23.47596703998600276, 11.44779298504227860 ) ) ;
#8261=ORIENTED_EDGE ( 'NONE', *, *, #37521, .T. ) ;
#8262=CARTESIAN_POINT ( 'NONE',  ( -58.58953762381673158, -24.65952944569304250, 1.056160979905698127 ) ) ;
#8264=CARTESIAN_POINT ( 'NONE',  ( -35.49720035677762553, -24.15602025860895452, 10.28564288303536856 ) ) ;
#8265=CARTESIAN_POINT ( 'NONE',  ( -15.06743543786183714, 14.52697759824333090, 11.49999999999998934 ) ) ;
#8266=ORIENTED_EDGE ( 'NONE', *, *, #24245, .F. ) ;
#8267=DIRECTION ( 'NONE',  ( 0.000000000000000000, -0.9999999999976377785, -2.173523156925979128E-06 ) ) ;
#8268=VERTEX_POINT ( 'NONE', #27641 ) ;
#8269=DIRECTION ( 'NONE',  ( 0.000000000000000000, -2.173523156925980399E-06, 0.9999999999976378895 ) ) ;
#8270=CARTESIAN_POINT ( 'NONE',  ( -15.68702345270385834, -14.21367052863537417, -1.500000000000002220 ) ) ;
#8271=ORIENTED_EDGE ( 'NONE', *, *, #19553, .F. ) ;
#8272=CARTESIAN_POINT ( 'NONE',  ( -50.58898002243636682, -24.52300882791530157, 0.6510814631126389251 ) ) ;
#8273=CARTESIAN_POINT ( 'NONE',  ( 19.81658424304261246, 9.080307684375437560, -1.500000000000002220 ) ) ;
#8274=DIRECTION ( 'NONE',  ( 0.000000000000000000, -2.173523156925979552E-06, 0.9999999999976378895 ) ) ;
#8275=CARTESIAN_POINT ( 'NONE',  ( -89.52287095715006160, -24.64965694238407323, 8.947790433994196491 ) ) ;
#8276=CARTESIAN_POINT ( 'NONE',  ( -75.52287095715006160, -25.00158670708909625, 2.256160236439166411 ) ) ;
#8277=CARTESIAN_POINT ( 'NONE',  ( -16.21501377034323710, -14.60173171477820198, -1.500000000000002220 ) ) ;
#8278=CARTESIAN_POINT ( 'NONE',  ( -30.57287095715005165, -23.78566233802480312, -0.9545366882134203035 ) ) ;
#8280=CARTESIAN_POINT ( 'NONE',  ( -76.62287095715007013, -24.66019654487199730, 8.947790411086128159 ) ) ;
#8281=CARTESIAN_POINT ( 'NONE',  ( -85.62363014113577719, -25.00182538069147142, 7.747789668545045139 ) ) ;
#8283=ORIENTED_EDGE ( 'NONE', *, *, #85738, .F. ) ;
#8284=ORIENTED_EDGE ( 'NONE', *, *, #42237, .T. ) ;
#8285=CARTESIAN_POINT ( 'NONE',  ( -89.40841769935764205, -25.12049752546738191, 2.832404795212221327 ) ) ;
#8286=CARTESIAN_POINT ( 'NONE',  ( -45.52287095715007581, -23.47593901973090169, -1.443836447538997092 ) ) ;
#8287=CARTESIAN_POINT ( 'NONE',  ( -6.347832186973104029, -20.24257907634199682, 11.49999999999998934 ) ) ;
#8288=CARTESIAN_POINT ( 'NONE',  ( -125.6228709571500559, -23.47593901973091235, -1.443836447538995760 ) ) ;
#8291=CARTESIAN_POINT ( 'NONE',  ( -99.52287095715011844, -24.33832256527049154, 0.1851278514138630094 ) ) ;
#8292=CARTESIAN_POINT ( 'NONE',  ( 4.312616920666290987, -18.91975033782923887, -1.500000000000002220 ) ) ;
#8293=EDGE_CURVE ( 'NONE', #11381, #34120, #13762, .T. ) ;
#8294=CARTESIAN_POINT ( 'NONE',  ( -41.88562729343752267, -25.32724636324323342, 4.398074533285874388 ) ) ;
#8295=ORIENTED_EDGE ( 'NONE', *, *, #19850, .F. ) ;
#8296=ADVANCED_FACE ( 'NONE', ( #81917 ), #37241, .T. ) ;
#8297=CARTESIAN_POINT ( 'NONE',  ( -17.86923650574433609, -7.721772263035739492, 11.49999999999999645 ) ) ;
#8298=CARTESIAN_POINT ( 'NONE',  ( -79.11611000704996854, -29.50249039766296022, 3.409318347773680369 ) ) ;
#8299=EDGE_CURVE ( 'NONE', #58944, #69140, #8925, .T. ) ;
#8304=CARTESIAN_POINT ( 'NONE',  ( -44.62287095715004881, -23.47593901973091235, -1.443836447539011525 ) ) ;
#8306=CARTESIAN_POINT ( 'NONE',  ( -106.5228709571500758, -24.64898659630368627, 1.056161002820831474 ) ) ;
#8307=CARTESIAN_POINT ( 'NONE',  ( -93.58413747110309089, -24.66019654487200441, 8.947790411086105067 ) ) ;
#8308=CARTESIAN_POINT ( 'NONE',  ( 5.239555828037883778, -18.94419173073049478, 11.49999999999998934 ) ) ;
#8309=LINE ( 'NONE', #39253, #65582 ) ;
#8310=ORIENTED_EDGE ( 'NONE', *, *, #30413, .T. ) ;
#8311=CARTESIAN_POINT ( 'NONE',  ( -7.206546067468990735, 20.34698395366585189, 11.49999999999998934 ) ) ;
#8312=CARTESIAN_POINT ( 'NONE',  ( -40.52054906611086693, -25.00158670708910336, 2.256160236439222366 ) ) ;
#8315=CARTESIAN_POINT ( 'NONE',  ( -20.34888222059871410, 10.79260868881566715, -1.500000000000002220 ) ) ;
#8319=CARTESIAN_POINT ( 'NONE',  ( -121.5537543563160625, -24.51419770103157347, 9.386484678747175181 ) ) ;
#8320=CARTESIAN_POINT ( 'NONE',  ( -90.62287095715004170, -29.50247984919015209, -1.443849546365051806 ) ) ;
#8321=CARTESIAN_POINT ( 'NONE',  ( -110.3139465455115129, -25.29823811160681046, 2.832404408888942626 ) ) ;
#8322=CARTESIAN_POINT ( 'NONE',  ( -127.6228709571500559, -29.50248528299804818, 1.056150453629047137 ) ) ;
#8323=CARTESIAN_POINT ( 'NONE',  ( -49.52287095715007581, -23.47593901973090169, -1.443836447538997092 ) ) ;
#8324=CARTESIAN_POINT ( 'NONE',  ( -1.646307629438301667, 19.86461321233117872, 11.49999999999998934 ) ) ;
#8325=CARTESIAN_POINT ( 'NONE',  ( -101.2005726979208617, -25.24249036930439871, 3.670115594759035371 ) ) ;
#8326=CARTESIAN_POINT ( 'NONE',  ( 17.96171645398845129, 8.431260308876343146, -1.500000000000002220 ) ) ;
#8330=CARTESIAN_POINT ( 'NONE',  ( -94.92287095715005307, -23.47593901973090169, -1.443836447538996870 ) ) ;
#8331=CARTESIAN_POINT ( 'NONE',  ( -13.51810693421681719, -15.76408947421354156, 11.49999999999999645 ) ) ;
#8334=CARTESIAN_POINT ( 'NONE',  ( -106.5126059859705379, -24.51314013834316441, 0.6176544820404206160 ) ) ;
#8335=CARTESIAN_POINT ( 'NONE',  ( -22.77908990650604792, -0.06651829912971220227, 11.49999999999999645 ) ) ;
#8337=CARTESIAN_POINT ( 'NONE',  ( -69.58051520251109423, -24.65952944569304606, 1.056160979905704567 ) ) ;
#8338=CARTESIAN_POINT ( 'NONE',  ( -70.01986906652584253, -25.12987166818711060, 7.062085323942192794 ) ) ;
#8340=CARTESIAN_POINT ( 'NONE',  ( 7.037473118728134303, -18.94123407977296480, -1.500000000000002220 ) ) ;
#8342=DIRECTION ( 'NONE',  ( -3.773278334453079618E-23, 0.9999999999976377785, 2.173523156925979975E-06 ) ) ;
#8344=B_SPLINE_CURVE_WITH_KNOTS ( 'NONE', 3,
 ( #333, #70351, #55137, #78947, #9445, #63764, #2349, #8450 ),
 .UNSPECIFIED., .F., .F.,
 ( 4, 2, 2, 4 ),
 ( 0.000000000000000000, 0.002001098010032679314, 0.003001647015049018971, 0.004002196020065358628 ),
 .UNSPECIFIED. ) ;
#8346=CARTESIAN_POINT ( 'NONE',  ( -127.5228709571500900, -23.96127896941632685, -0.6493128931037952523 ) ) ;
#8347=CARTESIAN_POINT ( 'NONE',  ( -7.509321099650855480, 21.62252279970214985, -1.500000000000002220 ) ) ;
#8348=CARTESIAN_POINT ( 'NONE',  ( -51.04387771620785941, -25.27420607828345567, 3.499820197422921719 ) ) ;
#8349=CARTESIAN_POINT ( 'NONE',  ( -8.642975711230413083, 19.83371042614930957, -1.500000000000002220 ) ) ;
#8350=DIRECTION ( 'NONE',  ( -1.000000000000000000, -3.773278334444166432E-23, -8.201307841325785021E-29 ) ) ;
#8351=CARTESIAN_POINT ( 'NONE',  ( -5.628781154649386664, 20.11113626451368219, 11.49999999999999645 ) ) ;
#8352=ORIENTED_EDGE ( 'NONE', *, *, #86480, .F. ) ;
#8354=CARTESIAN_POINT ( 'NONE',  ( -124.5202242993295982, -24.34968618360934300, 0.1864209137778899961 ) ) ;
#8355=CARTESIAN_POINT ( 'NONE',  ( -2.902263480631018577, 21.84654903556016947, 11.49999999999998934 ) ) ;
#8362=EDGE_CURVE ( 'NONE', #11149, #59077, #41666, .T. ) ;
#8364=B_SPLINE_CURVE_WITH_KNOTS ( 'NONE', 3,
 ( #91194, #97808, #21666, #45041 ),
 .UNSPECIFIED., .F., .F.,
 ( 4, 4 ),
 ( 0.000000000000000000, 9.999999999998897304E-05 ),
 .UNSPECIFIED. ) ;
#8366=CARTESIAN_POINT ( 'NONE',  ( -112.5228709571500616, -29.50248528299804818, 1.056150453629043584 ) ) ;
#8367=EDGE_LOOP ( 'NONE', ( #6618, #52808, #62295, #46064 ) ) ;
#8368=VERTEX_POINT ( 'NONE', #52971 ) ;
#8369=CARTESIAN_POINT ( 'NONE',  ( -71.63964193945945169, -23.96169478059713498, 10.65365249895718058 ) ) ;
#8370=CARTESIAN_POINT ( 'NONE',  ( -83.52287095715006160, -23.47596703998600631, 11.44779298504228571 ) ) ;
#8372=CARTESIAN_POINT ( 'NONE',  ( -16.05948562299510485, -12.68841425896798469, -1.500000000000002220 ) ) ;
#8373=EDGE_LOOP ( 'NONE', ( #95649, #92975, #64159, #92148 ) ) ;
#8374=CARTESIAN_POINT ( 'NONE',  ( -79.11611000704996854, -25.13069340115296058, 2.947789388436138580 ) ) ;
#8377=CARTESIAN_POINT ( 'NONE',  ( -3.941980378682776287, 21.93750326593198352, -1.500000000000002220 ) ) ;
#8378=CARTESIAN_POINT ( 'NONE',  ( -71.09433122556509943, -25.18619088944823758, 6.774128143594245088 ) ) ;
#8380=ORIENTED_EDGE ( 'NONE', *, *, #74911, .T. ) ;
#8381=LINE ( 'NONE', #46449, #3073 ) ;
#8382=CARTESIAN_POINT ( 'NONE',  ( -29.70813536620188700, -24.63645634153647990, 6.270928624350932346 ) ) ;
#8383=CARTESIAN_POINT ( 'NONE',  ( 13.71216040526616098, 15.69570726272272232, -1.500000000000002220 ) ) ;
#8385=ORIENTED_EDGE ( 'NONE', *, *, #91511, .F. ) ;
#8386=LINE ( 'NONE', #78383, #19542 ) ;
#8387=ORIENTED_EDGE ( 'NONE', *, *, #24455, .T. ) ;
#8389=CARTESIAN_POINT ( 'NONE',  ( -58.52287095715008292, -24.33927499327856125, 9.819080762295811837 ) ) ;
#8390=CARTESIAN_POINT ( 'NONE',  ( -20.11743356864677423, -6.099313207006018089, -1.500000000000002220 ) ) ;
#8392=PLANE ( 'NONE',  #44590 ) ;
#8395=DIRECTION ( 'NONE',  ( -1.000000000000000000, -3.773278334444167608E-23, -8.201307833595939069E-29 ) ) ;
#8396=CARTESIAN_POINT ( 'NONE',  ( -36.62287095715006302, -24.65952944569303895, 1.056160979905693909 ) ) ;
#8398=CARTESIAN_POINT ( 'NONE',  ( 2.577866586777615154, 22.04066829813923789, 11.49999999999999645 ) ) ;
#8399=VERTEX_POINT ( 'NONE', #63976 ) ;
#8402=ORIENTED_EDGE ( 'NONE', *, *, #99124, .T. ) ;
#8403=CARTESIAN_POINT ( 'NONE',  ( -22.35490716430079061, -3.811827842488555440, 11.49999999999998934 ) ) ;
#8405=CARTESIAN_POINT ( 'NONE',  ( -28.54669807489977273, -24.93252285695803749, 7.282279334780318969 ) ) ;
#8407=AXIS2_PLACEMENT_3D ( 'NONE', #20906, #21894, #52374 ) ;
#8408=ORIENTED_EDGE ( 'NONE', *, *, #62977, .F. ) ;
#8410=CARTESIAN_POINT ( 'NONE',  ( -70.52287095715007581, -29.50247984919015209, -1.443849546365055359 ) ) ;
#8411=B_SPLINE_CURVE_WITH_KNOTS ( 'NONE', 3,
 ( #89270, #96882, #11635, #43600, #42613, #21240 ),
 .UNSPECIFIED., .F., .F.,
 ( 4, 2, 4 ),
 ( 1.571326169170308057E-05, 0.001397068978785498622, 0.002778424695879294117 ),
 .UNSPECIFIED. ) ;
#8412=B_SPLINE_CURVE_WITH_KNOTS ( 'NONE', 3,
 ( #54090, #85011, #45971, #15495 ),
 .UNSPECIFIED., .F., .F.,
 ( 4, 4 ),
 ( 0.000000000000000000, 0.0001000000000000028644 ),
 .UNSPECIFIED. ) ;
#8413=CARTESIAN_POINT ( 'NONE',  ( 20.05498121024909253, 1.910150955369836812, 11.49999999999998934 ) ) ;
#8414=CARTESIAN_POINT ( 'NONE',  ( -101.6228709571500559, -29.50248528299804818, 1.056150453629042030 ) ) ;
#8418=CARTESIAN_POINT ( 'NONE',  ( -21.99995728619510516, 3.820703864638951952, -1.500000000000002220 ) ) ;
#8419=ORIENTED_EDGE ( 'NONE', *, *, #16444, .T. ) ;
#8421=CARTESIAN_POINT ( 'NONE',  ( -101.2134684488937069, -25.16257435076780169, 6.841542966572015771 ) ) ;
#8427=CARTESIAN_POINT ( 'NONE',  ( -95.52287095715006160, -24.99132157543166954, 2.256160258750667502 ) ) ;
#8428=CARTESIAN_POINT ( 'NONE',  ( -10.41718274906430786, -16.55731393670301088, -1.500000000000002220 ) ) ;
#8431=CARTESIAN_POINT ( 'NONE',  ( 18.54456287915894563, -10.88813254144886322, 11.49999999999998934 ) ) ;
#8432=CARTESIAN_POINT ( 'NONE',  ( -128.6235872204422321, -24.51314013834317862, 0.6176544820404316072 ) ) ;
#8433=EDGE_CURVE ( 'NONE', #83907, #62489, #97358, .T. ) ;
#8437=CARTESIAN_POINT ( 'NONE',  ( 4.459850365305920938, 22.40387240153798487, -1.500000000000002220 ) ) ;
#8438=AXIS2_PLACEMENT_3D ( 'NONE', #69817, #69315, #24133 ) ;
#8440=CARTESIAN_POINT ( 'NONE',  ( -120.5228709571500616, -25.00158670708909625, 2.256160236439166411 ) ) ;
#8441=CARTESIAN_POINT ( 'NONE',  ( -70.35895856474229504, -25.31161946917133321, 5.313173610579343453 ) ) ;
#8442=CARTESIAN_POINT ( 'NONE',  ( -1.415466703587968667, 19.98303252902060834, 11.49999999999999645 ) ) ;
#8443=CARTESIAN_POINT ( 'NONE',  ( -99.92287095715006728, -23.47593901973090169, -1.443836447538996870 ) ) ;
#8447=B_SPLINE_CURVE_WITH_KNOTS ( 'NONE', 3,
 ( #73701, #4196, #97531, #81314, #28029, #74205, #4695, #11796, #49384, #58988, #66120, #19407, #42284, #56995, #73214, #89428, #50376, #42770, #43755, #20392, #34649, #51367 ),
 .UNSPECIFIED., .F., .F.,
 ( 4, 2, 2, 2, 2, 2, 2, 2, 2, 2, 4 ),
 ( 0.000000000000000000, 0.0002789761287897273164, 0.0005579522575794546328, 0.0008369283863691820034, 0.001115904515158909266, 0.001673856772738364874, 0.002231809030317820700, 0.002789761287897275874, 0.003347713545476731917, 0.003905665803056187092, 0.004463618060635643134 ),
 .UNSPECIFIED. ) ;
#8448=ORIENTED_EDGE ( 'NONE', *, *, #59899, .F. ) ;
#8449=ADVANCED_FACE ( 'NONE', ( #48739 ), #72564, .F. ) ;
#8450=CARTESIAN_POINT ( 'NONE',  ( -85.62287095715004170, -24.99132157543083821, 2.256160258750667502 ) ) ;
#8451=CARTESIAN_POINT ( 'NONE',  ( 18.41774212405765709, -11.57998961627671441, -1.500000000000002220 ) ) ;
#8453=CARTESIAN_POINT ( 'NONE',  ( -17.62575346185542102, 8.740161020289619387, -1.500000000000002220 ) ) ;
#8454=DIRECTION ( 'NONE',  ( 0.000000000000000000, 0.9999999999976377785, 2.173523156925979128E-06 ) ) ;
#8455=FACE_OUTER_BOUND ( 'NONE', #79387, .T. ) ;
#8460=CARTESIAN_POINT ( 'NONE',  ( 4.814550503181614260, -19.98661186389175271, 11.49999999999999645 ) ) ;
#8464=CARTESIAN_POINT ( 'NONE',  ( -12.77507031947300042, 18.62636059118606724, 11.49999999999999645 ) ) ;
#8466=CARTESIAN_POINT ( 'NONE',  ( -99.55666892486131303, -25.26387334811825269, 4.188639845853757926 ) ) ;
#8467=CARTESIAN_POINT ( 'NONE',  ( -60.55620429048340014, -24.99132157543166599, 2.256160258750668390 ) ) ;
#8469=CARTESIAN_POINT ( 'NONE',  ( -85.62287095715007013, -25.00158670708909270, 2.256160236439165967 ) ) ;
#8470=CARTESIAN_POINT ( 'NONE',  ( -26.25023971703978276, -24.61459967487257217, 7.578547068710756562 ) ) ;
#8472=EDGE_CURVE ( 'NONE', #59266, #77504, #5338, .T. ) ;
#8475=CARTESIAN_POINT ( 'NONE',  ( 20.16173082093541424, 11.17373015621797627, 11.49999999999999645 ) ) ;
#8476=CARTESIAN_POINT ( 'NONE',  ( 9.312063170398973355, -20.82641193498425025, -1.500000000000002220 ) ) ;
#8477=CARTESIAN_POINT ( 'NONE',  ( -33.62287095715005592, -23.47596703998600276, 11.44779298504227505 ) ) ;
#8478=CARTESIAN_POINT ( 'NONE',  ( -105.6228709571500275, -23.84047902841604127, -0.8780736468305382347 ) ) ;
#8481=CARTESIAN_POINT ( 'NONE',  ( 22.29217321540274099, 2.676729263222305644, 11.49999999999999645 ) ) ;
#8482=VERTEX_POINT ( 'NONE', #74058 ) ;
#8483=CARTESIAN_POINT ( 'NONE',  ( -84.52287095715006160, -23.47593901973090524, -1.443836447538996648 ) ) ;
#8484=CARTESIAN_POINT ( 'NONE',  ( -38.62287095715005592, -24.64965695001467694, 8.947790433994187609 ) ) ;
#8485=CARTESIAN_POINT ( 'NONE',  ( -9.563806973793814947, 19.74097577964120376, 11.49999999999998934 ) ) ;
#8488=CARTESIAN_POINT ( 'NONE',  ( -71.52287095715007581, -23.48786465467241058, 11.44779295918254647 ) ) ;
#8489=CARTESIAN_POINT ( 'NONE',  ( -126.6228709571500559, -23.47593901973091235, -1.443836447538995760 ) ) ;
#8491=CARTESIAN_POINT ( 'NONE',  ( -78.54639593351097915, -24.34968618360933945, 0.1864209137778830849 ) ) ;
#8494=CARTESIAN_POINT ( 'NONE',  ( -20.44062828730913139, -1.133067592104922694, -1.500000000000002220 ) ) ;
#8498=ORIENTED_EDGE ( 'NONE', *, *, #66219, .F. ) ;
#8500=CARTESIAN_POINT ( 'NONE',  ( -17.29220519630379016, 15.29500218549028645, 11.49999999999998934 ) ) ;
#8501=CARTESIAN_POINT ( 'NONE',  ( -40.79740563987936497, -25.26871255744267231, 3.880430150159563496 ) ) ;
#8502=CARTESIAN_POINT ( 'NONE',  ( 16.58868386459195676, 11.68684615565071283, -1.500000000000002220 ) ) ;
#8505=CARTESIAN_POINT ( 'NONE',  ( -92.54897924172895785, -24.34968618360935011, 0.1864209137778966296 ) ) ;
#8506=PLANE ( 'NONE',  #33531 ) ;
#8508=CARTESIAN_POINT ( 'NONE',  ( -13.16228656746626591, 16.97819584282690286, 11.49999999999999645 ) ) ;
#8510=CARTESIAN_POINT ( 'NONE',  ( -75.65600191686841924, -23.48783264082477018, -1.443836473390089914 ) ) ;
#8511=CARTESIAN_POINT ( 'NONE',  ( -61.59803781195726913, -23.96169478059713143, 10.65365249895718591 ) ) ;
#8513=CARTESIAN_POINT ( 'NONE',  ( -18.06733440434376092, 10.15830956056102963, 11.49999999999998934 ) ) ;
#8514=ORIENTED_EDGE ( 'NONE', *, *, #33342, .F. ) ;
#8517=ORIENTED_EDGE ( 'NONE', *, *, #40410, .F. ) ;
#8519=CARTESIAN_POINT ( 'NONE',  ( -41.49211046241916989, -24.35071581493542681, 9.817618358456032368 ) ) ;
#8520=DIRECTION ( 'NONE',  ( -3.773278334453079030E-23, 0.9999999999976377785, 2.173523156925979128E-06 ) ) ;
#8522=ORIENTED_EDGE ( 'NONE', *, *, #19539, .F. ) ;
#8523=CARTESIAN_POINT ( 'NONE',  ( -40.52287095715007581, -24.15431212366391023, -0.2830839119429403028 ) ) ;
#8524=CARTESIAN_POINT ( 'NONE',  ( -77.62287095715004170, -23.72773821059535848, 11.05748984161097503 ) ) ;
#8525=CARTESIAN_POINT ( 'NONE',  ( -64.62287095715005592, -29.50248528299804818, 1.056150453629034924 ) ) ;
#8526=CARTESIAN_POINT ( 'NONE',  ( -21.99024891984110752, 1.279939690139831665, 11.49999999999999645 ) ) ;
#8528=CARTESIAN_POINT ( 'NONE',  ( -8.190886813464794969, 21.05079722441571732, 11.49999999999998934 ) ) ;
#8529=CARTESIAN_POINT ( 'NONE',  ( 2.184583272949580213, -20.89682302726931340, -1.500000000000002220 ) ) ;
#8531=CARTESIAN_POINT ( 'NONE',  ( -46.66198039096105532, -23.48786465467240703, 11.44779295918255180 ) ) ;
#8532=ORIENTED_EDGE ( 'NONE', *, *, #61268, .T. ) ;
#8533=B_SPLINE_CURVE_WITH_KNOTS ( 'NONE', 3,
 ( #75433, #98773, #68343, #20156 ),
 .UNSPECIFIED., .F., .F.,
 ( 4, 4 ),
 ( 0.000000000000000000, 0.0001000000000000028644 ),
 .UNSPECIFIED. ) ;
#8534=VECTOR ( 'NONE', #32149, 1000.000000000000114 ) ;
#8535=ORIENTED_EDGE ( 'NONE', *, *, #14481, .T. ) ;
#8536=CARTESIAN_POINT ( 'NONE',  ( -88.52287095715006160, -24.64965694238407323, 8.947790433994196491 ) ) ;
#8539=CARTESIAN_POINT ( 'NONE',  ( 10.59196434753715010, 18.29633683537252509, 11.49999999999998934 ) ) ;
#8541=CARTESIAN_POINT ( 'NONE',  ( -50.46940435010577630, -25.03148741713950187, 7.561692462087905575 ) ) ;
#8542=CARTESIAN_POINT ( 'NONE',  ( -88.62287095715004170, -24.64965695001469115, 8.947790433994180503 ) ) ;
#8545=CARTESIAN_POINT ( 'NONE',  ( -22.11311035156252558, 1.696007508605793301, -1.500000000000002220 ) ) ;
#8547=EDGE_CURVE ( 'NONE', #46190, #41589, #56228, .T. ) ;
#8549=CARTESIAN_POINT ( 'NONE',  ( -82.58953762381671027, -23.47596703998600276, 11.44779298504227683 ) ) ;
#8550=CARTESIAN_POINT ( 'NONE',  ( -37.64896086412395704, -23.96119346886880663, -0.6495511937831990323 ) ) ;
#8551=CARTESIAN_POINT ( 'NONE',  ( -40.33334756173746172, -25.30373406279863957, 5.539412886275527192 ) ) ;
#8552=CARTESIAN_POINT ( 'NONE',  ( -100.5847598729784380, -24.92564183028979130, 1.928384488918251760 ) ) ;
#8553=B_SPLINE_CURVE_WITH_KNOTS ( 'NONE', 3,
 ( #67553, #90872, #74644, #13238, #98471, #52818, #29463, #6633, #45704, #51826, #38081, #58935, #76630, #27981 ),
 .UNSPECIFIED., .F., .F.,
 ( 4, 2, 2, 2, 2, 2, 4 ),
 ( 8.673617379884035472E-19, 0.0001871047122523776312, 0.0003742094245047543951, 0.0007484188490095090070, 0.001122628273514263836, 0.001309732985766650900, 0.001496837698019038180 ),
 .UNSPECIFIED. ) ;
#8554=DIRECTION ( 'NONE',  ( 1.000000000000000000, 3.773278334444167608E-23, 8.201307833595939069E-29 ) ) ;
#8555=VECTOR ( 'NONE', #29401, 1000.000000000000114 ) ;
#8556=CARTESIAN_POINT ( 'NONE',  ( -0.2416374764669896869, -19.45557994585427508, 11.49999999999998934 ) ) ;
#8558=EDGE_CURVE ( 'NONE', #53441, #90740, #6594, .T. ) ;
#8559=CARTESIAN_POINT ( 'NONE',  ( -21.12015818079280649, -3.594773940630530795, 11.49999999999998934 ) ) ;
#8560=CARTESIAN_POINT ( 'NONE',  ( -64.55620429048339304, -24.65952944569304606, 1.056160979905695685 ) ) ;
#8561=CARTESIAN_POINT ( 'NONE',  ( -60.58056880734444860, -24.83644354574317603, 8.397322867105112110 ) ) ;
#8563=CARTESIAN_POINT ( 'NONE',  ( -51.54141383909072971, -24.34968618360933590, 0.1864209137778788938 ) ) ;
#8564=CARTESIAN_POINT ( 'NONE',  ( -44.52287095715006160, -24.64965694238575011, 8.947790433994205372 ) ) ;
#8565=CARTESIAN_POINT ( 'NONE',  ( -1.179572987637725889, 22.66035800735570049, -1.500000000000002220 ) ) ;
#8566=VECTOR ( 'NONE', #60261, 1000.000000000000114 ) ;
#8567=PLANE ( 'NONE',  #85462 ) ;
#8569=CARTESIAN_POINT ( 'NONE',  ( 17.96171645398845129, 8.431260308876343146, 11.49999999999999645 ) ) ;
#8572=CARTESIAN_POINT ( 'NONE',  ( -73.62287095715008434, -24.33832256526968862, 0.1851278514119885088 ) ) ;
#8574=ORIENTED_EDGE ( 'NONE', *, *, #20459, .T. ) ;
#8576=DIRECTION ( 'NONE',  ( -1.000000000000000000, -3.773278334444167608E-23, -8.201307833595939069E-29 ) ) ;
#8578=CARTESIAN_POINT ( 'NONE',  ( -51.32120688873476411, -25.27412302063908101, 3.174475563666860012 ) ) ;
#8579=CARTESIAN_POINT ( 'NONE',  ( -20.21959982808627032, -7.803091810188320210, 11.49999999999998934 ) ) ;
#8580=CARTESIAN_POINT ( 'NONE',  ( -32.58953762381672448, -24.66019654487198665, 8.947790411086138818 ) ) ;
#8581=CARTESIAN_POINT ( 'NONE',  ( -10.96721834449554933, 16.09610527815933168, -1.500000000000002220 ) ) ;
#8582=CARTESIAN_POINT ( 'NONE',  ( -61.62287095715008434, -23.95044443724992433, 10.65354141964650125 ) ) ;
#8583=VERTEX_POINT ( 'NONE', #75036 ) ;
#8584=CARTESIAN_POINT ( 'NONE',  ( 19.80222353126469415, -4.898785079568316547, 11.49999999999999645 ) ) ;
#8585=CARTESIAN_POINT ( 'NONE',  ( -80.58515248380662399, -24.73486907724918282, 1.287355809206963908 ) ) ;
#8586=CARTESIAN_POINT ( 'NONE',  ( -69.62287095715005592, -29.50250243563736774, 8.947779886222143375 ) ) ;
#8589=CARTESIAN_POINT ( 'NONE',  ( -79.23479724101613897, -25.14774951949591042, 6.961175731640159015 ) ) ;
#8590=CARTESIAN_POINT ( 'NONE',  ( -29.62287095715004881, -24.58390616985635546, 1.056161279468100123 ) ) ;
#8591=DIRECTION ( 'NONE',  ( -3.773278334453079030E-23, 0.9999999999976377785, 2.173523156925979128E-06 ) ) ;
#8592=CARTESIAN_POINT ( 'NONE',  ( -40.62957167911499567, -24.83644354573577928, 8.397322867130096569 ) ) ;
#8594=CARTESIAN_POINT ( 'NONE',  ( -3.374260732160392795, -19.82512954709321562, -1.500000000000002220 ) ) ;
#8599=CARTESIAN_POINT ( 'NONE',  ( -95.62287095715005592, -24.99156045073393173, 7.747789690856161648 ) ) ;
#8600=ADVANCED_FACE ( 'NONE', ( #83653 ), #20251, .F. ) ;
#8601=CARTESIAN_POINT ( 'NONE',  ( 2.319610639010541764, -22.79860127089448696, 11.49999999999999645 ) ) ;
#8602=B_SPLINE_CURVE_WITH_KNOTS ( 'NONE', 3,
 ( #41017, #10552, #41511, #95789, #62682, #30208 ),
 .UNSPECIFIED., .F., .F.,
 ( 4, 2, 4 ),
 ( 0.000000000000000000, 0.001380764517854762364, 0.002761529035709524727 ),
 .UNSPECIFIED. ) ;
#8603=CARTESIAN_POINT ( 'NONE',  ( -22.07869367785253090, -5.390224856484156390, -1.500000000000002220 ) ) ;
#8604=VERTEX_POINT ( 'NONE', #20749 ) ;
#8605=CARTESIAN_POINT ( 'NONE',  ( -71.70487185728066493, -25.24836947220651595, 6.282845680122700394 ) ) ;
#8606=VECTOR ( 'NONE', #69359, 1000.000000000000114 ) ;
#8607=LINE ( 'NONE', #93835, #65609 ) ;
#8608=CARTESIAN_POINT ( 'NONE',  ( -39.44867388513146977, -25.28405637431412956, 4.124821700262499391 ) ) ;
#8609=CARTESIAN_POINT ( 'NONE',  ( -30.57287095715005876, -24.68108607773119090, 1.119903471769779335 ) ) ;
#8610=CARTESIAN_POINT ( 'NONE',  ( -128.5561025708502143, -23.73791477778912551, 11.05961554403169522 ) ) ;
#8612=CARTESIAN_POINT ( 'NONE',  ( -40.52287095715006870, -23.47593901973090169, -1.443836447538997092 ) ) ;
#8614=CARTESIAN_POINT ( 'NONE',  ( -2.125485521908593078, 20.27274140177646444, 11.49999999999998934 ) ) ;
#8616=CARTESIAN_POINT ( 'NONE',  ( 18.09022303007301247, 14.20294132079179938, 11.49999999999998934 ) ) ;
#8618=DIRECTION ( 'NONE',  ( -2.860369681942282691E-39, -2.173523156925979128E-06, 0.9999999999976378895 ) ) ;
#8620=DIRECTION ( 'NONE',  ( 1.000000000000000000, 3.773278334444166432E-23, 8.201307841325785021E-29 ) ) ;
#8622=CARTESIAN_POINT ( 'NONE',  ( -118.7289294252545488, -25.23516544469813283, 6.311314093648517698 ) ) ;
#8623=CARTESIAN_POINT ( 'NONE',  ( 20.65877813657638740, 5.380652674160894655, 11.49999999999999645 ) ) ;
#8624=ORIENTED_EDGE ( 'NONE', *, *, #33867, .F. ) ;
#8626=ORIENTED_EDGE ( 'NONE', *, *, #88602, .T. ) ;
#8627=CARTESIAN_POINT ( 'NONE',  ( -5.994446910899359438, -21.39327697068355505, -1.500000000000002220 ) ) ;
#8628=CARTESIAN_POINT ( 'NONE',  ( 19.46067915675286386, 6.892634557253153105, -1.500000000000002220 ) ) ;
#8629=ADVANCED_FACE ( 'NONE', ( #6540 ), #30368, .F. ) ;
#8632=DIRECTION ( 'NONE',  ( -3.773278334444166432E-23, 1.000000000000000000, 0.000000000000000000 ) ) ;
#8633=CARTESIAN_POINT ( 'NONE',  ( -95.54869878359860991, -24.52399227489127398, 9.353111116836524630 ) ) ;
#8634=ORIENTED_EDGE ( 'NONE', *, *, #60014, .F. ) ;
#8638=VECTOR ( 'NONE', #99622, 1000.000000000000114 ) ;
#8640=CARTESIAN_POINT ( 'NONE',  ( -116.2228709571500644, -23.47596703998600631, 11.44779298504227860 ) ) ;
#8641=CARTESIAN_POINT ( 'NONE',  ( -19.94048968823238255, 6.179419890754223488, -1.500000000000002220 ) ) ;
#8642=CARTESIAN_POINT ( 'NONE',  ( 16.32745387341675780, -14.53119815553504068, 11.49999999999999645 ) ) ;
#8643=CARTESIAN_POINT ( 'NONE',  ( -27.27372260060660736, -24.89279990012216359, 7.541612528384861847 ) ) ;
#8644=CARTESIAN_POINT ( 'NONE',  ( -98.97737064162744502, -25.20109320840395739, 6.595599656366546881 ) ) ;
#8645=CARTESIAN_POINT ( 'NONE',  ( 6.846561153812083411, -21.39451737393737574, 11.49999999999998934 ) ) ;
#8646=EDGE_CURVE ( 'NONE', #71422, #52694, #15031, .T. ) ;
#8647=EDGE_CURVE ( 'NONE', #52813, #12728, #23457, .T. ) ;
#8648=CARTESIAN_POINT ( 'NONE',  ( -50.41800648699645393, -25.26334751556140290, 4.735576037500227820 ) ) ;
#8649=CARTESIAN_POINT ( 'NONE',  ( -50.52287095715006160, -23.48786465467241058, 11.44779295918255002 ) ) ;
#8651=B_SPLINE_SURFACE_WITH_KNOTS ( 'NONE', 3, 3, ( 
 ( #73474, #19172, #57760, #27299 ),
 ( #89200, #72985, #2468, #43029 ),
 ( #80083, #35420, #73972, #96309 ),
 ( #71986, #34412, #41033, #80580 ),
 ( #81085, #33402, #64394, #4470 ),
 ( #11561, #50634, #18674, #25797 ),
 ( #42539, #66379, #64894, #95309 ) ),
 .UNSPECIFIED., .F., .F., .F.,
 ( 4, 3, 4 ),
 ( 4, 4 ),
 ( 0.2590395444657082047, 0.4996700994841927201, 0.7403006545026772356 ),
 ( 0.9757605720749513711, 0.9935688618463752730 ),
 .UNSPECIFIED. ) ;
#8652=B_SPLINE_CURVE_WITH_KNOTS ( 'NONE', 3,
 ( #36503, #4070, #50746, #89800 ),
 .UNSPECIFIED., .F., .F.,
 ( 4, 4 ),
 ( 2.775557561562891351E-17, 0.0001000000000000028644 ),
 .UNSPECIFIED. ) ;
#8654=VERTEX_POINT ( 'NONE', #83151 ) ;
#8656=CARTESIAN_POINT ( 'NONE',  ( -17.20161093224466953, -12.68000408521323408, -1.500000000000002220 ) ) ;
#8657=CARTESIAN_POINT ( 'NONE',  ( 12.67250375155129127, 18.46511205475877304, 11.49999999999999645 ) ) ;
#8659=CARTESIAN_POINT ( 'NONE',  ( -21.07084664159375009, 0.3847054351051909515, 11.49999999999998934 ) ) ;
#8660=CARTESIAN_POINT ( 'NONE',  ( -67.62287095715005592, -29.50250243563736774, 8.947779886222143375 ) ) ;
#8661=CARTESIAN_POINT ( 'NONE',  ( -16.62890364678930410, -10.96057169749504645, -1.500000000000002220 ) ) ;
#8662=CARTESIAN_POINT ( 'NONE',  ( -50.52684220265726367, -24.92592662359561473, 8.075495903018000021 ) ) ;
#8663=CARTESIAN_POINT ( 'NONE',  ( -49.25197268407241324, -25.13168855254613021, 7.110315888415422947 ) ) ;
#8664=CARTESIAN_POINT ( 'NONE',  ( -13.73438224071023761, 17.16576579689093762, -1.500000000000002220 ) ) ;
#8665=CARTESIAN_POINT ( 'NONE',  ( -84.52287095715006160, -24.64965694238406613, 8.947790433994198267 ) ) ;
#8667=CARTESIAN_POINT ( 'NONE',  ( -74.55620429048335041, -24.64965694238574301, 8.947790433994201820 ) ) ;
#8670=CARTESIAN_POINT ( 'NONE',  ( -81.62287095715005592, -29.50248528299804818, 1.056150453629038477 ) ) ;
#8671=CARTESIAN_POINT ( 'NONE',  ( 13.71216040526616098, 15.69570726272272232, 11.49999999999999645 ) ) ;
#8674=FACE_OUTER_BOUND ( 'NONE', #21224, .T. ) ;
#8675=CARTESIAN_POINT ( 'NONE',  ( -117.5228709571500758, -24.65952944569305316, 1.056160979905705899 ) ) ;
#8676=CARTESIAN_POINT ( 'NONE',  ( -1.376967878889499897, 21.29249089469206524, -1.500000000000002220 ) ) ;
#8678=CARTESIAN_POINT ( 'NONE',  ( -48.62287095715004881, -29.50250786944525672, 11.44777988621624054 ) ) ;
#8679=ADVANCED_FACE ( 'NONE', ( #44107 ), #6034, .F. ) ;
#8680=CARTESIAN_POINT ( 'NONE',  ( -64.49195876600683164, -24.66019654487199730, 8.947790411086113949 ) ) ;
#8681=CARTESIAN_POINT ( 'NONE',  ( -69.99588697226764111, -25.12112739299269037, 7.112216829152949948 ) ) ;
#8682=CARTESIAN_POINT ( 'NONE',  ( -6.869692127560369066, -21.44495933931894527, -1.500000000000002220 ) ) ;
#8683=EDGE_CURVE ( 'NONE', #80402, #73900, #61061, .T. ) ;
#8686=B_SPLINE_CURVE_WITH_KNOTS ( 'NONE', 3,
 ( #36793, #67755, #35306, #60148 ),
 .UNSPECIFIED., .F., .F.,
 ( 4, 4 ),
 ( 0.5709076711935395787, 0.5799141024656551124 ),
 .UNSPECIFIED. ) ;
#8687=CARTESIAN_POINT ( 'NONE',  ( -99.22287095715007865, -23.47593901973090524, -1.443836447538996870 ) ) ;
#8688=CARTESIAN_POINT ( 'NONE',  ( -31.62374207134597270, -24.66019654487199020, 8.947790411086133489 ) ) ;
#8689=CARTESIAN_POINT ( 'NONE',  ( -19.15281226579456231, 4.489446101945751444, 11.49999999999999645 ) ) ;
#8692=ORIENTED_EDGE ( 'NONE', *, *, #98529, .T. ) ;
#8693=EDGE_CURVE ( 'NONE', #70837, #76528, #90776, .T. ) ;
#8695=CARTESIAN_POINT ( 'NONE',  ( -75.62287095715005592, -29.50250786944525672, 11.44777988621623521 ) ) ;
#8696=LINE ( 'NONE', #93918, #53105 ) ;
#8698=CARTESIAN_POINT ( 'NONE',  ( -40.52287095715006870, -29.50248528299804818, 1.056150453629031594 ) ) ;
#8700=CARTESIAN_POINT ( 'NONE',  ( 14.33573519231038063, 13.56928687979844561, -1.500000000000002220 ) ) ;
#8702=ORIENTED_EDGE ( 'NONE', *, *, #53860, .T. ) ;
#8707=CARTESIAN_POINT ( 'NONE',  ( -70.27422298781921484, -25.30465073045868252, 4.851635164186505200 ) ) ;
#8709=CARTESIAN_POINT ( 'NONE',  ( -80.77170908772370694, -25.30559281118826220, 4.999461766569205601 ) ) ;
#8713=VECTOR ( 'NONE', #85666, 1000.000000000000114 ) ;
#8715=CARTESIAN_POINT ( 'NONE',  ( 11.47056939498152950, -16.38825109899074661, 11.49999999999998934 ) ) ;
#8716=CARTESIAN_POINT ( 'NONE',  ( -34.58953762381672448, -24.64898659630367206, 1.056161002820377393 ) ) ;
#8717=PLANE ( 'NONE',  #28981 ) ;
#8718=VERTEX_POINT ( 'NONE', #53223 ) ;
#8720=CARTESIAN_POINT ( 'NONE',  ( -79.58202135401835164, -24.66019654487199375, 8.947790411086119278 ) ) ;
#8721=CARTESIAN_POINT ( 'NONE',  ( -109.3584176993576591, -25.29012923716278749, 4.206202503440089835 ) ) ;
#8722=CARTESIAN_POINT ( 'NONE',  ( -35.64597012725812419, -24.40034930558991277, 0.3402023900116170063 ) ) ;
#8723=CARTESIAN_POINT ( 'NONE',  ( -108.5228709571500900, -24.33832256527048798, 0.1851278514138625098 ) ) ;
#8724=B_SPLINE_CURVE_WITH_KNOTS ( 'NONE', 3,
 ( #85192, #47149, #46649, #77568 ),
 .UNSPECIFIED., .F., .F.,
 ( 4, 4 ),
 ( 1.387778780781445676E-17, 9.999999999997510880E-05 ),
 .UNSPECIFIED. ) ;
#8725=CARTESIAN_POINT ( 'NONE',  ( -119.4728709570019589, -25.40556189117671693, 4.803963375099986166 ) ) ;
#8726=FACE_OUTER_BOUND ( 'NONE', #10506, .T. ) ;
#8730=CARTESIAN_POINT ( 'NONE',  ( 20.05935882324986963, -3.104462954613115500, 11.49999999999998934 ) ) ;
#8733=CARTESIAN_POINT ( 'NONE',  ( -59.53433122793244081, -24.66019654487199730, 8.947790411086124607 ) ) ;
#8734=ORIENTED_EDGE ( 'NONE', *, *, #51282, .F. ) ;
#8736=CARTESIAN_POINT ( 'NONE',  ( -18.21026628907936029, 8.684577975296603469, -1.500000000000002220 ) ) ;
#8737=AXIS2_PLACEMENT_3D ( 'NONE', #9230, #48821, #78232 ) ;
#8738=CARTESIAN_POINT ( 'NONE',  ( 1.363997202867437863, 21.09336101032836908, 11.49999999999999645 ) ) ;
#8739=CARTESIAN_POINT ( 'NONE',  ( -15.83042281971428977, -15.45127431894796466, 11.49999999999998934 ) ) ;
#8740=CARTESIAN_POINT ( 'NONE',  ( -20.42507745660439156, -2.452541965221147535, 11.49999999999998934 ) ) ;
#8741=EDGE_CURVE ( 'NONE', #79654, #71653, #42919, .T. ) ;
#8742=CARTESIAN_POINT ( 'NONE',  ( -60.58057154149170032, -24.83618233451449697, 1.606449574219536380 ) ) ;
#8743=ORIENTED_EDGE ( 'NONE', *, *, #13912, .F. ) ;
#8744=CARTESIAN_POINT ( 'NONE',  ( -32.62287095715004881, -23.72747288104469732, -1.053458166803227902 ) ) ;
#8746=CARTESIAN_POINT ( 'NONE',  ( -57.62287095715004881, -23.48786465467241058, 11.44779295918254824 ) ) ;
#8749=EDGE_LOOP ( 'NONE', ( #24867, #52643, #28795 ) ) ;
#8751=CARTESIAN_POINT ( 'NONE',  ( -110.3139465455115271, -25.12049752546738191, 2.832404795212222659 ) ) ;
#8754=CARTESIAN_POINT ( 'NONE',  ( -19.50335911044312098, -6.847048061534898977, -1.500000000000002220 ) ) ;
#8755=CARTESIAN_POINT ( 'NONE',  ( 9.217229664113554932, 19.63635308506117383, 11.49999999999999645 ) ) ;
#8757=EDGE_CURVE ( 'NONE', #29214, #76528, #36792, .T. ) ;
#8758=CARTESIAN_POINT ( 'NONE',  ( -46.55620429048337883, -24.64965694238575011, 8.947790433994201820 ) ) ;
#8760=CARTESIAN_POINT ( 'NONE',  ( -11.14805103425725719, -19.39388463112642214, 11.49999999999998934 ) ) ;
#8763=CARTESIAN_POINT ( 'NONE',  ( -79.39179774623507058, -25.12205638436979882, 6.303984304149410356 ) ) ;
#8764=CARTESIAN_POINT ( 'NONE',  ( -101.5228709571500474, -24.33927499327855415, 9.819080762295810061 ) ) ;
#8766=CARTESIAN_POINT ( 'NONE',  ( -118.3652930134189774, -25.31861658550455374, 6.462000913474522434 ) ) ;
#8767=CARTESIAN_POINT ( 'NONE',  ( -35.65499668529189137, -24.15602025860895452, 10.28564288303536856 ) ) ;
#8769=VERTEX_POINT ( 'NONE', #31877 ) ;
#8770=CARTESIAN_POINT ( 'NONE',  ( -45.52287095715006870, -24.62285846331438677, 9.038163153548225637 ) ) ;
#8772=CARTESIAN_POINT ( 'NONE',  ( -109.5151415522008023, -24.35071581493543391, 9.817618358456025263 ) ) ;
#8773=CARTESIAN_POINT ( 'NONE',  ( -16.93204426113827310, 12.72334981527875186, -1.500000000000002220 ) ) ;
#8774=ORIENTED_EDGE ( 'NONE', *, *, #17458, .F. ) ;
#8776=CARTESIAN_POINT ( 'NONE',  ( -3.204121956075930200, -21.57847171274271858, 11.49999999999998934 ) ) ;
#8777=CARTESIAN_POINT ( 'NONE',  ( -113.6228709571500417, -23.47596703998600631, 11.44779298504227860 ) ) ;
#8778=FACE_OUTER_BOUND ( 'NONE', #16752, .T. ) ;
#8779=CARTESIAN_POINT ( 'NONE',  ( -116.6228709571500417, -24.51283580621365843, 0.6167428607019838083 ) ) ;
#8780=CARTESIAN_POINT ( 'NONE',  ( 6.711561834375728175, -20.75310922853297058, -1.500000000000002220 ) ) ;
#8784=CARTESIAN_POINT ( 'NONE',  ( -85.55841537188921109, -23.85049219812685450, 10.88485053497527133 ) ) ;
#8787=ORIENTED_EDGE ( 'NONE', *, *, #81249, .F. ) ;
#8791=CARTESIAN_POINT ( 'NONE',  ( -120.2228709571500644, -23.47593901973090524, -1.443836447538996426 ) ) ;
#8792=CARTESIAN_POINT ( 'NONE',  ( -20.47598858559898716, 5.595549388561865456, 11.49999999999998934 ) ) ;
#8793=CARTESIAN_POINT ( 'NONE',  ( -121.6228709571500843, -23.94994826722515668, -0.6494450866351686447 ) ) ;
#8795=AXIS2_PLACEMENT_3D ( 'NONE', #11087, #81601, #3489 ) ;
#8797=CARTESIAN_POINT ( 'NONE',  ( -42.52287095715005449, -29.50247984919015209, -1.443849546365060466 ) ) ;
#8798=DIRECTION ( 'NONE',  ( 3.773278334444166432E-23, -1.000000000000000000, 0.000000000000000000 ) ) ;
#8799=CARTESIAN_POINT ( 'NONE',  ( 2.844571010020486845, -19.19604305453586690, -1.500000000000002220 ) ) ;
#8800=CARTESIAN_POINT ( 'NONE',  ( -40.93937950312512442, -25.11539320593059443, 2.804431443241629740 ) ) ;
#8802=CARTESIAN_POINT ( 'NONE',  ( 4.731349760756693890, 18.90081699332259646, 11.49999999999999645 ) ) ;
#8805=ORIENTED_EDGE ( 'NONE', *, *, #36622, .F. ) ;
#8808=CARTESIAN_POINT ( 'NONE',  ( -58.62287095715005592, -24.33927499327854704, 9.819080762295822495 ) ) ;
#8809=DIRECTION ( 'NONE',  ( -3.773278334453079618E-23, 0.9999999999976377785, 2.173523156925979975E-06 ) ) ;
#8810=CARTESIAN_POINT ( 'NONE',  ( -106.5228709571500900, -23.72747288104470442, -1.053458166803224794 ) ) ;
#8812=CARTESIAN_POINT ( 'NONE',  ( -93.55195563180954821, -24.15620529776628800, 10.23563542870659582 ) ) ;
#8813=CARTESIAN_POINT ( 'NONE',  ( 16.09843989366402539, -11.26760994518913428, 11.49999999999998934 ) ) ;
#8814=CARTESIAN_POINT ( 'NONE',  ( -117.6228709571500559, -24.51387760970724372, 9.387446482453409402 ) ) ;
#8816=CARTESIAN_POINT ( 'NONE',  ( -18.50814150397365410, 11.09706937414969374, -1.500000000000002220 ) ) ;
#8817=LINE ( 'NONE', #61623, #83071 ) ;
#8819=CARTESIAN_POINT ( 'NONE',  ( 23.08992502549420323, -0.8469403905869224980, -1.500000000000002220 ) ) ;
#8821=CARTESIAN_POINT ( 'NONE',  ( -93.63360391309790032, -23.96119346886880663, -0.6495511937832079141 ) ) ;
#8822=CARTESIAN_POINT ( 'NONE',  ( -90.52287095715006160, -23.84081130425357387, 10.88220057483158243 ) ) ;
#8823=PLANE ( 'NONE',  #10456 ) ;
#8825=CARTESIAN_POINT ( 'NONE',  ( -111.7148472136480990, -25.10921600246400587, 3.873546110135351217 ) ) ;
#8826=CARTESIAN_POINT ( 'NONE',  ( -124.6228709571500559, -23.48786465467241769, 11.44779295918253759 ) ) ;
#8827=CARTESIAN_POINT ( 'NONE',  ( -114.5530339053627813, -24.35071581493544457, 9.817618358456016381 ) ) ;
#8828=CARTESIAN_POINT ( 'NONE',  ( -19.91179686852411734, 0.6080443046932394457, -1.500000000000002220 ) ) ;
#8829=CARTESIAN_POINT ( 'NONE',  ( -75.54218285077926964, -24.63419186844611275, 9.035850630976923981 ) ) ;
#8830=CARTESIAN_POINT ( 'NONE',  ( -19.81728208556213389, 0.3677575464312098363, -1.500000000000002220 ) ) ;
#8832=CARTESIAN_POINT ( 'NONE',  ( -39.32379795506943054, -25.10925708289683911, 3.365606678701691834 ) ) ;
#8835=CARTESIAN_POINT ( 'NONE',  ( -16.75865769207039335, -12.26659692683164593, 11.49999999999999645 ) ) ;
#8836=PLANE ( 'NONE',  #41925 ) ;
#8837=CARTESIAN_POINT ( 'NONE',  ( -106.5874661333381397, -24.51314013834316796, 0.6176544820404221703 ) ) ;
#8838=CARTESIAN_POINT ( 'NONE',  ( -21.15473383059569557, 8.456223909384457116, 11.49999999999999645 ) ) ;
#8840=CARTESIAN_POINT ( 'NONE',  ( -91.62287095715004170, -24.64898659630368627, 1.056161002820827921 ) ) ;
#8841=CARTESIAN_POINT ( 'NONE',  ( -69.34303308397305443, -25.24554880456021522, 6.209207408033732278 ) ) ;
#8843=CARTESIAN_POINT ( 'NONE',  ( -19.21899500656021331, -6.280627263257740900, 11.49999999999998934 ) ) ;
#8844=PLANE ( 'NONE',  #79191 ) ;
#8846=ORIENTED_EDGE ( 'NONE', *, *, #27384, .F. ) ;
#8847=DIRECTION ( 'NONE',  ( 0.000000000000000000, -0.9999999999976377785, -2.173523156925979128E-06 ) ) ;
#8848=CARTESIAN_POINT ( 'NONE',  ( 0.5590224530292132732, -22.91010021869659852, 11.49999999999998934 ) ) ;
#8849=CARTESIAN_POINT ( 'NONE',  ( -50.43601667505130592, -25.27420563262489139, 3.294780489091903686 ) ) ;
#8850=CARTESIAN_POINT ( 'NONE',  ( 18.80801646011137507, -6.797914457553222434, -1.500000000000002220 ) ) ;
#8851=CARTESIAN_POINT ( 'NONE',  ( -41.26959558397305727, -25.07899898050004950, 7.338714981574760543 ) ) ;
#8852=CARTESIAN_POINT ( 'NONE',  ( -20.44905293368100985, -4.654758753755802836, 11.49999999999999645 ) ) ;
#8854=CARTESIAN_POINT ( 'NONE',  ( -86.62287095715001328, -23.47596703998600631, 11.44779298504227683 ) ) ;
#8855=CARTESIAN_POINT ( 'NONE',  ( -124.5888236901737969, -24.65952944569305316, 1.056160979905708563 ) ) ;
#8856=CARTESIAN_POINT ( 'NONE',  ( -7.037580251249667462, -20.86201633182841420, -1.500000000000002220 ) ) ;
#8860=B_SPLINE_CURVE_WITH_KNOTS ( 'NONE', 3,
 ( #38470, #8524, #62322, #23736, #47096, #73923 ),
 .UNSPECIFIED., .F., .F.,
 ( 4, 2, 4 ),
 ( 0.000000000000000000, 0.001380901958385384641, 0.002761803916770769283 ),
 .UNSPECIFIED. ) ;
#8861=CARTESIAN_POINT ( 'NONE',  ( -49.86550021440504565, -25.18440128170155035, 3.414711424454316191 ) ) ;
#8862=CARTESIAN_POINT ( 'NONE',  ( -126.6228709571500559, -29.50247984919015209, -1.443849546365044922 ) ) ;
#8863=ORIENTED_EDGE ( 'NONE', *, *, #65199, .F. ) ;
#8865=EDGE_CURVE ( 'NONE', #95482, #3899, #33186, .T. ) ;
#8870=CARTESIAN_POINT ( 'NONE',  ( -101.0021142486707646, -25.27404655521463184, 2.948027157395776587 ) ) ;
#8871=CARTESIAN_POINT ( 'NONE',  ( -36.53267038383642529, -24.51314013834317151, 0.6176544820404150649 ) ) ;
#8872=CARTESIAN_POINT ( 'NONE',  ( -18.14515864413662172, 9.488524743509296755, -1.500000000000002220 ) ) ;
#8873=B_SPLINE_CURVE_WITH_KNOTS ( 'NONE', 3,
 ( #7172, #7680, #18789, #93913 ),
 .UNSPECIFIED., .F., .F.,
 ( 4, 4 ),
 ( 0.000000000000000000, 9.999999999998897304E-05 ),
 .UNSPECIFIED. ) ;
#8874=AXIS2_PLACEMENT_3D ( 'NONE', #33718, #4270, #11870 ) ;
#8877=PLANE ( 'NONE',  #88270 ) ;
#8878=CARTESIAN_POINT ( 'NONE',  ( -44.52977088278382922, -24.65952944569304606, 1.056160979905693909 ) ) ;
#8879=CARTESIAN_POINT ( 'NONE',  ( -40.45829750704998418, -25.18492896333868103, 3.293943116708551777 ) ) ;
#8880=CARTESIAN_POINT ( 'NONE',  ( 22.30035941410032763, -0.3387204123245128873, 11.49999999999998934 ) ) ;
#8881=EDGE_CURVE ( 'NONE', #36540, #54139, #61340, .T. ) ;
#8882=CARTESIAN_POINT ( 'NONE',  ( -70.62782063829519075, -25.14001972948981134, 7.062078543324224356 ) ) ;
#8883=CARTESIAN_POINT ( 'NONE',  ( -27.51755584304929414, -24.62734232575839144, 8.245802515575128666 ) ) ;
#8884=EDGE_LOOP ( 'NONE', ( #92043, #16100, #98962, #74650 ) ) ;
#8885=CARTESIAN_POINT ( 'NONE',  ( -28.07868692527382493, -24.64332086767980101, 1.662177252415085293 ) ) ;
#8886=CARTESIAN_POINT ( 'NONE',  ( -73.52287095715007581, -24.65952944569304606, 1.056160979905697239 ) ) ;
#8887=CARTESIAN_POINT ( 'NONE',  ( -12.81329989551134751, 16.42372500408851366, -1.500000000000002220 ) ) ;
#8892=CARTESIAN_POINT ( 'NONE',  ( -31.52287095715006160, -24.65952944569304606, 1.056160979905690134 ) ) ;
#8893=CARTESIAN_POINT ( 'NONE',  ( 0.9685562702117149758, 20.96446713366763248, -1.500000000000002220 ) ) ;
#8894=VERTEX_POINT ( 'NONE', #54227 ) ;
#8896=CARTESIAN_POINT ( 'NONE',  ( -53.52287095715007581, -24.33927499327856125, 9.819080762295815390 ) ) ;
#8898=CARTESIAN_POINT ( 'NONE',  ( -101.6175123368144142, -25.03152335046257448, 7.038108615052007799 ) ) ;
#8899=CARTESIAN_POINT ( 'NONE',  ( -60.62287095715004881, -24.14406661707768365, 10.28769366152059739 ) ) ;
#8900=CARTESIAN_POINT ( 'NONE',  ( -64.52287095715006160, -23.47596703998600631, 11.44779298504228926 ) ) ;
#8901=CARTESIAN_POINT ( 'NONE',  ( -18.13406196532287140, 12.77545654309102474, 11.49999999999999645 ) ) ;
#8903=LINE ( 'NONE', #39849, #33982 ) ;
#8905=ORIENTED_EDGE ( 'NONE', *, *, #59755, .T. ) ;
#8906=CARTESIAN_POINT ( 'NONE',  ( 12.64511023617726160, -18.80563239904246231, -1.500000000000002220 ) ) ;
#8907=LINE ( 'NONE', #25122, #36085 ) ;
#8909=VERTEX_POINT ( 'NONE', #15642 ) ;
#8912=CARTESIAN_POINT ( 'NONE',  ( -14.30055291515510518, -14.21740073472259525, -1.500000000000002220 ) ) ;
#8913=FACE_OUTER_BOUND ( 'NONE', #20132, .T. ) ;
#8914=ORIENTED_EDGE ( 'NONE', *, *, #78625, .T. ) ;
#8915=CARTESIAN_POINT ( 'NONE',  ( -92.55620429048340725, -23.48786465467241413, 11.44779295918254292 ) ) ;
#8916=CARTESIAN_POINT ( 'NONE',  ( 0.2029947971921062799, -22.41465419638480228, -1.500000000000002220 ) ) ;
#8920=CARTESIAN_POINT ( 'NONE',  ( -94.58861374093797281, -24.35071581493543036, 9.817618358456030592 ) ) ;
#8921=CARTESIAN_POINT ( 'NONE',  ( -35.52287095715006870, -29.50249982740957577, 7.747779886224967605 ) ) ;
#8922=CARTESIAN_POINT ( 'NONE',  ( -89.40841769935767047, -29.50248914370730091, 2.832395270851967073 ) ) ;
#8923=CARTESIAN_POINT ( 'NONE',  ( -97.25938467801201170, -23.78062553189672812, -0.9709657327914289482 ) ) ;
#8924=EDGE_CURVE ( 'NONE', #91672, #71483, #31371, .T. ) ;
#8925=B_SPLINE_CURVE_WITH_KNOTS ( 'NONE', 3,
 ( #38225, #46345, #21990, #30114, #14884, #1554 ),
 .UNSPECIFIED., .F., .F.,
 ( 4, 2, 4 ),
 ( 0.000000000000000000, 0.001380764517853247083, 0.002761529035706494165 ),
 .UNSPECIFIED. ) ;
#8926=CARTESIAN_POINT ( 'NONE',  ( 2.510080532074158377, -19.39449211012750496, 11.49999999999998934 ) ) ;
#8929=CARTESIAN_POINT ( 'NONE',  ( 21.49998558720804809, 0.1351929536555107336, 11.49999999999998934 ) ) ;
#8930=CARTESIAN_POINT ( 'NONE',  ( -62.52287095715009002, -24.51387760970724372, 9.387446482453405849 ) ) ;
#8935=CARTESIAN_POINT ( 'NONE',  ( 17.95915693031428262, 14.28781372813260120, -1.500000000000002220 ) ) ;
#8938=CARTESIAN_POINT ( 'NONE',  ( -120.6228709571500701, -25.00158670708909625, 2.256160236439166411 ) ) ;
#8939=CARTESIAN_POINT ( 'NONE',  ( -92.62287095715005592, -23.47593901973091235, -1.443836447539002865 ) ) ;
#8940=CARTESIAN_POINT ( 'NONE',  ( 14.85562765054232059, -13.46834898924134372, 11.49999999999999645 ) ) ;
#8941=CARTESIAN_POINT ( 'NONE',  ( -79.04068788000392942, -25.31594508206281802, 5.390100702044224867 ) ) ;
#8946=CARTESIAN_POINT ( 'NONE',  ( -65.62287095715005592, -23.47593901973091235, -1.443836447539006196 ) ) ;
#8947=AXIS2_PLACEMENT_3D ( 'NONE', #58463, #48852, #10274 ) ;
#8948=CARTESIAN_POINT ( 'NONE',  ( -19.00758693998263738, -10.61793046214600089, -1.500000000000002220 ) ) ;
#8950=CARTESIAN_POINT ( 'NONE',  ( -11.91260469445801995, 15.66180005371307260, -1.500000000000002220 ) ) ;
#8953=B_SPLINE_CURVE_WITH_KNOTS ( 'NONE', 3,
 ( #45382, #58599, #66736, #74806, #37260, #60610, #12409, #28151 ),
 .UNSPECIFIED., .F., .F.,
 ( 4, 2, 2, 4 ),
 ( 6.391158118972243699E-06, 0.002007136338672931355, 0.003007508928949908632, 0.004007881519226886777 ),
 .UNSPECIFIED. ) ;
#8954=DIRECTION ( 'NONE',  ( 0.000000000000000000, -2.173523156925979552E-06, 0.9999999999976378895 ) ) ;
#8957=CARTESIAN_POINT ( 'NONE',  ( -6.092534927433182368, -19.63929903328317295, 11.49999999999999645 ) ) ;
#8959=DIRECTION ( 'NONE',  ( -3.773278334453079618E-23, 0.9999999999976377785, 2.173523156925978705E-06 ) ) ;
#8960=CARTESIAN_POINT ( 'NONE',  ( 19.70651319644445465, -11.07993823016455792, 11.49999999999999645 ) ) ;
#8962=FACE_OUTER_BOUND ( 'NONE', #51305, .T. ) ;
#8964=CARTESIAN_POINT ( 'NONE',  ( -125.6238069808063642, -24.83644354573579349, 8.397322867130096569 ) ) ;
#8966=B_SPLINE_CURVE_WITH_KNOTS ( 'NONE', 3,
 ( #40156, #32541, #87837, #17821 ),
 .UNSPECIFIED., .F., .F.,
 ( 4, 4 ),
 ( 2.791380378375079153E-06, 0.0004665020696472202692 ),
 .UNSPECIFIED. ) ;
#8967=CARTESIAN_POINT ( 'NONE',  ( -25.74405688418818272, -24.93063286172094450, 6.647229298724505853 ) ) ;
#8969=ORIENTED_EDGE ( 'NONE', *, *, #94638, .T. ) ;
#8970=CARTESIAN_POINT ( 'NONE',  ( 22.95697726795019378, -2.620641032420567118, 11.49999999999999645 ) ) ;
#8971=CARTESIAN_POINT ( 'NONE',  ( 21.82588152991271713, 6.770963248321698380, -1.500000000000002220 ) ) ;
#8973=CARTESIAN_POINT ( 'NONE',  ( -96.58868282968654739, -24.34968618360933945, 0.1864209137778869152 ) ) ;
#8974=CARTESIAN_POINT ( 'NONE',  ( -82.56324868667182670, -23.48786465467241413, 11.44779295918254824 ) ) ;
#8976=CARTESIAN_POINT ( 'NONE',  ( 3.503984654965784706, -22.18958196551723816, 11.49999999999999645 ) ) ;
#8978=FACE_OUTER_BOUND ( 'NONE', #3453, .T. ) ;
#8979=CARTESIAN_POINT ( 'NONE',  ( -21.09739860443290382, 5.981408608369527258, 11.49999999999998934 ) ) ;
#8981=CARTESIAN_POINT ( 'NONE',  ( -34.64979159594478375, -23.96169478059712077, 10.65365249895718769 ) ) ;
#8982=CARTESIAN_POINT ( 'NONE',  ( -121.5228709571500758, -24.33927499327855770, 9.819080762295813614 ) ) ;
#8983=ORIENTED_EDGE ( 'NONE', *, *, #1858, .F. ) ;
#8984=CARTESIAN_POINT ( 'NONE',  ( -48.65308815567226475, -23.73791477778911840, 11.05961554403170766 ) ) ;
#8986=ORIENTED_EDGE ( 'NONE', *, *, #20791, .F. ) ;
#8987=EDGE_CURVE ( 'NONE', #18949, #56586, #65358, .T. ) ;
#8988=CARTESIAN_POINT ( 'NONE',  ( -20.02755620033356010, -4.236777897013602079, 11.49999999999998934 ) ) ;
#8993=CARTESIAN_POINT ( 'NONE',  ( 10.36671515591691950, -20.60271000134967068, 11.49999999999998934 ) ) ;
#8995=CARTESIAN_POINT ( 'NONE',  ( -19.79944955726156763, -4.570829099900970860, -1.500000000000002220 ) ) ;
#8996=EDGE_CURVE ( 'NONE', #97579, #48183, #83849, .T. ) ;
#8998=CARTESIAN_POINT ( 'NONE',  ( -97.52287095715006160, -24.64965694238575011, 8.947790433994194714 ) ) ;
#8999=CARTESIAN_POINT ( 'NONE',  ( -73.52287095715007581, -23.48786465467241058, 11.44779295918254647 ) ) ;
#9001=DIRECTION ( 'NONE',  ( 3.773278334444167608E-23, -1.000000000000000000, 0.000000000000000000 ) ) ;
#9002=CARTESIAN_POINT ( 'NONE',  ( -70.53236091209835479, -25.00158670708910691, 2.256160236439221034 ) ) ;
#9003=CARTESIAN_POINT ( 'NONE',  ( 16.66814584454133907, -13.58961022886752978, 11.49999999999999645 ) ) ;
#9004=EDGE_LOOP ( 'NONE', ( #27987, #90613, #13601, #33123 ) ) ;
#9005=CARTESIAN_POINT ( 'NONE',  ( -79.55620429048339304, -24.66019654487199375, 8.947790411086131712 ) ) ;
#9006=CARTESIAN_POINT ( 'NONE',  ( -104.6228709571500559, -23.47593901973091235, -1.443836447539001089 ) ) ;
#9007=EDGE_CURVE ( 'NONE', #31838, #96235, #92308, .T. ) ;
#9010=CARTESIAN_POINT ( 'NONE',  ( 18.38559056850662543, 9.607341378227904016, 11.49999999999998934 ) ) ;
#9011=ORIENTED_EDGE ( 'NONE', *, *, #61711, .T. ) ;
#9012=CARTESIAN_POINT ( 'NONE',  ( -125.5543386547933977, -24.83618233451450763, 1.606449574219537046 ) ) ;
#9013=VERTEX_POINT ( 'NONE', #42998 ) ;
#9015=CARTESIAN_POINT ( 'NONE',  ( -111.5936678842673331, -23.73791477778912551, 11.05961554403170055 ) ) ;
#9017=ORIENTED_EDGE ( 'NONE', *, *, #90910, .T. ) ;
#9019=CARTESIAN_POINT ( 'NONE',  ( -58.87764846858842560, -29.50248939449842922, 2.947779886236309377 ) ) ;
#9020=CARTESIAN_POINT ( 'NONE',  ( -42.62869147627655053, -24.51419770103158413, 9.386484678747191168 ) ) ;
#9022=ADVANCED_FACE ( 'NONE', ( #12031 ), #95774, .F. ) ;
#9023=CARTESIAN_POINT ( 'NONE',  ( -29.36337478090402797, -24.98585162628100420, 2.615322239748779420 ) ) ;
#9024=CARTESIAN_POINT ( 'NONE',  ( 16.65356921002588919, 14.36988287374134821, 11.49999999999999645 ) ) ;
#9027=CARTESIAN_POINT ( 'NONE',  ( -17.80605238980536953, 13.89162706601689479, -1.500000000000002220 ) ) ;
#9028=CARTESIAN_POINT ( 'NONE',  ( 6.892386425805808514, -19.84609432511738447, 11.49999999999998934 ) ) ;
#9030=ORIENTED_EDGE ( 'NONE', *, *, #94900, .T. ) ;
#9032=DIRECTION ( 'NONE',  ( 0.000000000000000000, -2.173523156925979552E-06, 0.9999999999976378895 ) ) ;
#9033=CARTESIAN_POINT ( 'NONE',  ( -90.62287095715005592, -24.62285846362216546, 9.038163152653526211 ) ) ;
#9035=CARTESIAN_POINT ( 'NONE',  ( 20.98173926746349238, 2.650078317256617577, -1.500000000000002220 ) ) ;
#9037=CARTESIAN_POINT ( 'NONE',  ( -51.32936205048392964, -25.26041064547814941, 7.321355772070240242 ) ) ;
#9038=CARTESIAN_POINT ( 'NONE',  ( -121.5192093918902572, -24.34968618360933945, 0.1864209137778886083 ) ) ;
#9039=LINE ( 'NONE', #84661, #2208 ) ;
#9040=CARTESIAN_POINT ( 'NONE',  ( -101.5228709571501327, -23.96127896941632329, -0.6493128931038008034 ) ) ;
#9041=CARTESIAN_POINT ( 'NONE',  ( -4.073883676365832152, 21.86232641878667593, -1.500000000000002220 ) ) ;
#9042=FACE_OUTER_BOUND ( 'NONE', #21629, .T. ) ;
#9045=CARTESIAN_POINT ( 'NONE',  ( -51.26059310326842677, -25.24860019069869210, 5.062966105152178820 ) ) ;
#9047=FACE_OUTER_BOUND ( 'NONE', #11042, .T. ) ;
#9048=EDGE_CURVE ( 'NONE', #73282, #75171, #93551, .T. ) ;
#9051=CARTESIAN_POINT ( 'NONE',  ( 18.45204572605500104, 6.281640480902235701, -1.500000000000002220 ) ) ;
#9053=CARTESIAN_POINT ( 'NONE',  ( -20.52298544035203776, 6.160189734329080125, -1.500000000000002220 ) ) ;
#9054=CARTESIAN_POINT ( 'NONE',  ( -85.52287095715004739, -24.62285846331436190, 9.038163153548291362 ) ) ;
#9056=PLANE ( 'NONE',  #34147 ) ;
#9058=CARTESIAN_POINT ( 'NONE',  ( 17.68435195917723490, -14.24712819257710095, -1.500000000000002220 ) ) ;
#9059=B_SPLINE_CURVE_WITH_KNOTS ( 'NONE', 3,
 ( #28657, #59121, #92045, #44392 ),
 .UNSPECIFIED., .F., .F.,
 ( 4, 4 ),
 ( 0.4408147750407612198, 0.4498212063128765870 ),
 .UNSPECIFIED. ) ;
#9061=CARTESIAN_POINT ( 'NONE',  ( -103.6228709571500417, -24.65952944569304606, 1.056160979905701680 ) ) ;
#9062=CARTESIAN_POINT ( 'NONE',  ( -80.52287095715004739, -24.62226745350437440, 0.9660975649728149595 ) ) ;
#9063=CARTESIAN_POINT ( 'NONE',  ( 19.75055111929153639, -1.948201398878238066, 11.49999999999999645 ) ) ;
#9064=CARTESIAN_POINT ( 'NONE',  ( -61.64687923781919210, -25.21083105912962452, 3.409327675794633361 ) ) ;
#9065=CARTESIAN_POINT ( 'NONE',  ( -112.5562042904833788, -23.47596703998600631, 11.44779298504227683 ) ) ;
#9066=LINE ( 'NONE', #25287, #26138 ) ;
#9067=ORIENTED_EDGE ( 'NONE', *, *, #26020, .F. ) ;
#9068=DIRECTION ( 'NONE',  ( -3.773278334453079618E-23, 0.9999999999976377785, 2.173523156925979975E-06 ) ) ;
#9071=CARTESIAN_POINT ( 'NONE',  ( -51.69439593370608321, -25.10935976765677324, 3.842802501644153157 ) ) ;
#9072=CARTESIAN_POINT ( 'NONE',  ( -1.126084586642228436, -21.63456646517454729, 11.49999999999998934 ) ) ;
#9074=CARTESIAN_POINT ( 'NONE',  ( 18.70946937610417038, -5.484834493922766896, -1.500000000000002220 ) ) ;
#9075=PLANE ( 'NONE',  #86348 ) ;
#9076=ORIENTED_EDGE ( 'NONE', *, *, #29037, .F. ) ;
#9077=CARTESIAN_POINT ( 'NONE',  ( 4.102729645046709450, 19.96921287702725323, 11.49999999999999645 ) ) ;
#9078=DIRECTION ( 'NONE',  ( 0.000000000000000000, -0.9999999999976377785, -2.173523156925979975E-06 ) ) ;
#9081=CARTESIAN_POINT ( 'NONE',  ( -104.5895376238167245, -23.48783264082478794, -1.443836473390062158 ) ) ;
#9082=ORIENTED_EDGE ( 'NONE', *, *, #14418, .T. ) ;
#9084=CARTESIAN_POINT ( 'NONE',  ( -29.62287095715006302, -24.43673626876299920, 0.6166258652147375008 ) ) ;
#9085=CARTESIAN_POINT ( 'NONE',  ( -39.49170631829002787, -25.31628713280249698, 5.433214320636030159 ) ) ;
#9086=CARTESIAN_POINT ( 'NONE',  ( -40.48563153939314674, -24.52399227489126687, 9.353111116836521077 ) ) ;
#9088=LINE ( 'NONE', #92319, #96470 ) ;
#9089=CARTESIAN_POINT ( 'NONE',  ( 20.09017895974002599, 0.4902201509063087159, 11.49999999999998934 ) ) ;
#9091=FACE_OUTER_BOUND ( 'NONE', #6919, .T. ) ;
#9092=ORIENTED_EDGE ( 'NONE', *, *, #67213, .T. ) ;
#9093=CARTESIAN_POINT ( 'NONE',  ( -66.58367953917903037, -24.51419770103157347, 9.386484678747176957 ) ) ;
#9095=CARTESIAN_POINT ( 'NONE',  ( 2.177599385301639323, -22.86303409451243596, 11.49999999999999645 ) ) ;
#9096=CARTESIAN_POINT ( 'NONE',  ( 13.97002500213282516, -17.90638934399130733, -1.500000000000002220 ) ) ;
#9098=CARTESIAN_POINT ( 'NONE',  ( -30.47287095715006089, -25.28806803508177836, 5.559097854862454113 ) ) ;
#9100=CARTESIAN_POINT ( 'NONE',  ( -38.54595511171842759, -24.15620529776627379, 10.23563542870660825 ) ) ;
#9101=CARTESIAN_POINT ( 'NONE',  ( -30.57287095715008007, -24.05861711713197337, -0.4619017001958101165 ) ) ;
#9102=CARTESIAN_POINT ( 'NONE',  ( -128.5222656221514228, -23.48786465467242124, 11.44779295918253403 ) ) ;
#9103=CARTESIAN_POINT ( 'NONE',  ( -49.51489430277374026, -25.31544969143762458, 5.069408439402988797 ) ) ;
#9104=CARTESIAN_POINT ( 'NONE',  ( -61.52287095715006160, -24.64898659630367916, 1.056161002820822592 ) ) ;
#9105=CARTESIAN_POINT ( 'NONE',  ( -58.65645660196261701, -23.48783264082476663, -1.443836473390093689 ) ) ;
#9106=VERTEX_POINT ( 'NONE', #26264 ) ;
#9107=CARTESIAN_POINT ( 'NONE',  ( -14.54385459823299875, 14.27422344363935025, -1.500000000000002220 ) ) ;
#9109=EDGE_CURVE ( 'NONE', #13730, #96161, #40995, .T. ) ;
#9110=CARTESIAN_POINT ( 'NONE',  ( -0.3492834940180428727, 22.98956000712751546, 11.49999999999998934 ) ) ;
#9115=CARTESIAN_POINT ( 'NONE',  ( -81.62287095715004170, -24.66019654487199020, 8.947790411086131712 ) ) ;
#9116=CARTESIAN_POINT ( 'NONE',  ( -116.4728709571500360, -25.30558663486635140, 5.000950659935019971 ) ) ;
#9117=CARTESIAN_POINT ( 'NONE',  ( -20.14006130340733236, -7.001243683211865410, 11.49999999999999645 ) ) ;
#9119=EDGE_CURVE ( 'NONE', #36250, #94475, #36589, .T. ) ;
#9121=CARTESIAN_POINT ( 'NONE',  ( -13.56020932195406203, -17.60290058955388659, -1.500000000000002220 ) ) ;
#9122=ADVANCED_FACE ( 'NONE', ( #65854 ), #28687, .T. ) ;
#9123=CARTESIAN_POINT ( 'NONE',  ( 1.453578435135240321, -20.60874541997745268, -1.500000000000002220 ) ) ;
#9125=DIRECTION ( 'NONE',  ( 0.000000000000000000, 0.9999999999976377785, 2.173523156925979128E-06 ) ) ;
#9126=CARTESIAN_POINT ( 'NONE',  ( -95.58938763694557395, -24.52399227489127398, 9.353111116836521077 ) ) ;
#9128=CARTESIAN_POINT ( 'NONE',  ( -79.52287095715006160, -23.48786465467241058, 11.44779295918254469 ) ) ;
#9129=ORIENTED_EDGE ( 'NONE', *, *, #49574, .T. ) ;
#9130=DIRECTION ( 'NONE',  ( -3.773278334453079618E-23, 0.9999999999976377785, 2.173523156925979975E-06 ) ) ;
#9131=CARTESIAN_POINT ( 'NONE',  ( 6.973883220674568229, 19.69035807221911938, -1.500000000000002220 ) ) ;
#9133=CARTESIAN_POINT ( 'NONE',  ( 4.919149715316761373, 21.27959583485438344, 11.49999999999999645 ) ) ;
#9134=FACE_OUTER_BOUND ( 'NONE', #36227, .T. ) ;
#9135=DIRECTION ( 'NONE',  ( 0.000000000000000000, -0.9999999999976377785, -2.173523156925979128E-06 ) ) ;
#9136=CARTESIAN_POINT ( 'NONE',  ( 16.76845895467136671, -15.01613412638008782, -1.500000000000002220 ) ) ;
#9138=CARTESIAN_POINT ( 'NONE',  ( -50.47686723370601669, -25.26334751266341883, 4.734242724451897644 ) ) ;
#9139=CARTESIAN_POINT ( 'NONE',  ( -108.8968792378192063, -25.15277794460069316, 6.986250878905963191 ) ) ;
#9142=VERTEX_POINT ( 'NONE', #20636 ) ;
#9143=ORIENTED_EDGE ( 'NONE', *, *, #28431, .T. ) ;
#9146=CARTESIAN_POINT ( 'NONE',  ( -0.4629837013611828866, -21.40787533109759977, -1.500000000000002220 ) ) ;
#9147=CARTESIAN_POINT ( 'NONE',  ( -22.37156870845955225, 0.5457896250522937809, 11.49999999999999645 ) ) ;
#9148=EDGE_LOOP ( 'NONE', ( #82745, #22395, #30961, #9840 ) ) ;
#9149=CARTESIAN_POINT ( 'NONE',  ( 18.71565868802652588, -9.641079743366450572, 11.49999999999998934 ) ) ;
#9150=CARTESIAN_POINT ( 'NONE',  ( -30.40154523107553075, -25.30205729935985559, 3.857144010898052588 ) ) ;
#9151=CARTESIAN_POINT ( 'NONE',  ( 19.59856454566043382, -3.714209461170434157, -1.500000000000002220 ) ) ;
#9152=CARTESIAN_POINT ( 'NONE',  ( -50.53590823224938333, -24.63419186844610209, 9.035850630976920428 ) ) ;
#9155=CARTESIAN_POINT ( 'NONE',  ( -11.61111146657235871, -18.70866699758865792, -1.500000000000002220 ) ) ;
#9156=CARTESIAN_POINT ( 'NONE',  ( -83.52287095715007581, -23.72747288104470087, -1.053458166803226348 ) ) ;
#9158=B_SPLINE_CURVE_WITH_KNOTS ( 'NONE', 3,
 ( #85600, #22188, #7980, #14586 ),
 .UNSPECIFIED., .F., .F.,
 ( 4, 4 ),
 ( 0.000000000000000000, 9.999999999998897304E-05 ),
 .UNSPECIFIED. ) ;
#9161=CARTESIAN_POINT ( 'NONE',  ( 18.76864855846692492, -9.085702381504452418, 11.49999999999999645 ) ) ;
#9163=EDGE_CURVE ( 'NONE', #98076, #7900, #68055, .T. ) ;
#9166=CARTESIAN_POINT ( 'NONE',  ( -38.62287095715005592, -24.51387760970723662, 9.387446482453427166 ) ) ;
#9167=CARTESIAN_POINT ( 'NONE',  ( -17.77299844720193533, 11.79293508692305537, -1.500000000000002220 ) ) ;
#9168=CARTESIAN_POINT ( 'NONE',  ( -55.62287095715006302, -23.48786465467240703, 11.44779295918255180 ) ) ;
#9169=CARTESIAN_POINT ( 'NONE',  ( -51.08434323850904235, -25.22609634996768690, 3.528234306468502446 ) ) ;
#9171=CARTESIAN_POINT ( 'NONE',  ( -108.8968792378191921, -25.06732983082694943, 7.447789526168955732 ) ) ;
#9172=PLANE ( 'NONE',  #5445 ) ;
#9173=CARTESIAN_POINT ( 'NONE',  ( 16.76845895467136671, -15.01613412638008782, -1.500000000000002220 ) ) ;
#9174=CARTESIAN_POINT ( 'NONE',  ( -89.23534077628075067, -25.23397913219355004, 6.409327625488847602 ) ) ;
#9176=CARTESIAN_POINT ( 'NONE',  ( -98.62287095715005592, -23.47593901973091235, -1.443836447539001089 ) ) ;
#9177=CARTESIAN_POINT ( 'NONE',  ( -31.61027363099887921, -23.73791477778911130, 11.05961554403171299 ) ) ;
#9178=CARTESIAN_POINT ( 'NONE',  ( -14.15603575923578283, -13.64839490926926580, 11.49999999999999645 ) ) ;
#9180=CARTESIAN_POINT ( 'NONE',  ( -119.5228709571501184, -24.33927499327856125, 9.819080762295806508 ) ) ;
#9181=ORIENTED_EDGE ( 'NONE', *, *, #13025, .T. ) ;
#9182=CARTESIAN_POINT ( 'NONE',  ( -99.58680609741216472, -24.51314013834316796, 0.6176544820404258340 ) ) ;
#9183=LINE ( 'NONE', #8695, #77208 ) ;
#9184=CARTESIAN_POINT ( 'NONE',  ( -124.6251032423319032, -23.96169478059714564, 10.65365249895717170 ) ) ;
#9187=CARTESIAN_POINT ( 'NONE',  ( 7.891737972721761807, -18.10977644326358771, 11.49999999999998934 ) ) ;
#9190=CARTESIAN_POINT ( 'NONE',  ( 19.32837167043147986, -5.866312143582237404, 11.49999999999999645 ) ) ;
#9192=EDGE_CURVE ( 'NONE', #5846, #27769, #59612, .T. ) ;
#9193=VERTEX_POINT ( 'NONE', #5420 ) ;
#9199=CARTESIAN_POINT ( 'NONE',  ( -107.5862556121689835, -24.65952944569304606, 1.056160979905704789 ) ) ;
#9200=CARTESIAN_POINT ( 'NONE',  ( 13.83478396660306942, -14.44641118834825910, -1.500000000000002220 ) ) ;
#9202=CARTESIAN_POINT ( 'NONE',  ( -116.5517184843068890, -24.66019654487199730, 8.947790411086115725 ) ) ;
#9205=CARTESIAN_POINT ( 'NONE',  ( -79.63744741913833991, -23.96169478059713143, 10.65365249895718058 ) ) ;
#9206=DIRECTION ( 'NONE',  ( 0.000000000000000000, -2.173523156925980399E-06, 0.9999999999976378895 ) ) ;
#9207=CARTESIAN_POINT ( 'NONE',  ( -70.34543693012690824, -25.03284467579916495, 7.563174216508125269 ) ) ;
#9210=CARTESIAN_POINT ( 'NONE',  ( -83.58529744386720495, -24.51314013834315020, 0.6176544820404096248 ) ) ;
#9211=CARTESIAN_POINT ( 'NONE',  ( -49.62287095715005592, -29.50250243563736774, 8.947779886222146928 ) ) ;
#9212=CARTESIAN_POINT ( 'NONE',  ( -73.62287095715009855, -24.51283580621364067, 0.6167428607019832532 ) ) ;
#9214=ORIENTED_EDGE ( 'NONE', *, *, #69830, .F. ) ;
#9216=CARTESIAN_POINT ( 'NONE',  ( 17.43904876784772284, 10.37648870149486413, 11.49999999999998934 ) ) ;
#9217=EDGE_CURVE ( 'NONE', #35380, #56311, #44491, .T. ) ;
#9219=CARTESIAN_POINT ( 'NONE',  ( -34.61897583861063765, -23.48783264082478084, -1.443836473390076591 ) ) ;
#9220=CARTESIAN_POINT ( 'NONE',  ( -105.6228709571500559, -24.83602698348160942, 1.605859176311272618 ) ) ;
#9222=CARTESIAN_POINT ( 'NONE',  ( -50.40445135320379677, -25.12215419635199964, 7.101635560852263218 ) ) ;
#9223=CARTESIAN_POINT ( 'NONE',  ( 19.91930514195032487, 3.327535025408205893, -1.500000000000002220 ) ) ;
#9224=CARTESIAN_POINT ( 'NONE',  ( 20.45381123341165619, -5.387677532796200097, 11.49999999999999645 ) ) ;
#9225=CARTESIAN_POINT ( 'NONE',  ( -4.315754209668272168, 21.71352930684897942, -1.500000000000002220 ) ) ;
#9227=CARTESIAN_POINT ( 'NONE',  ( -15.41819309731374510, 13.62919173607049927, 11.49999999999998934 ) ) ;
#9230=CARTESIAN_POINT ( 'NONE',  ( -88.62287095715004170, -29.50248528299804818, 1.056150453629040253 ) ) ;
#9234=CARTESIAN_POINT ( 'NONE',  ( -109.5228709571500616, -24.64965694238408034, 8.947790433994192938 ) ) ;
#9237=VERTEX_POINT ( 'NONE', #52598 ) ;
#9239=CARTESIAN_POINT ( 'NONE',  ( -127.6228709571500843, -23.96177878511309345, 10.65340807706328974 ) ) ;
#9241=CARTESIAN_POINT ( 'NONE',  ( 20.01179378540625819, 5.277757631783551950, -1.500000000000002220 ) ) ;
#9243=CARTESIAN_POINT ( 'NONE',  ( 18.84366469573077296, 10.75509914293975555, 11.49999999999999645 ) ) ;
#9244=ORIENTED_EDGE ( 'NONE', *, *, #12994, .T. ) ;
#9245=CARTESIAN_POINT ( 'NONE',  ( -41.92287095715005307, -23.47596703998600276, 11.44779298504227683 ) ) ;
#9247=CARTESIAN_POINT ( 'NONE',  ( -111.0639896554701949, -25.14418962453571638, 3.027308487689960970 ) ) ;
#9248=CARTESIAN_POINT ( 'NONE',  ( 22.37589550080693712, 1.095942408959037273, -1.500000000000002220 ) ) ;
#9250=CARTESIAN_POINT ( 'NONE',  ( -79.34796103478946350, -25.27874851471385753, 6.000419794089626002 ) ) ;
#9251=CARTESIAN_POINT ( 'NONE',  ( -120.6228709571500275, -23.84081130438200802, 10.88220057463248658 ) ) ;
#9252=ORIENTED_EDGE ( 'NONE', *, *, #13634, .F. ) ;
#9254=CARTESIAN_POINT ( 'NONE',  ( -76.62287095715007013, -24.50321055353805377, 9.387540953477529371 ) ) ;
#9258=CARTESIAN_POINT ( 'NONE',  ( -110.2228709571500502, -23.47596703998600631, 11.44779298504227860 ) ) ;
#9260=DIRECTION ( 'NONE',  ( 0.000000000000000000, -0.9999999999976377785, -2.173523156925979975E-06 ) ) ;
#9261=CARTESIAN_POINT ( 'NONE',  ( -4.771770383141621608, -20.67029057396967318, -1.500000000000002220 ) ) ;
#9262=VERTEX_POINT ( 'NONE', #37377 ) ;
#9263=CARTESIAN_POINT ( 'NONE',  ( -117.5520258364394692, -24.65952944569305316, 1.056160979905706343 ) ) ;
#9264=CARTESIAN_POINT ( 'NONE',  ( -21.80608713477256089, -0.9339522974687717305, 11.49999999999998934 ) ) ;
#9265=CARTESIAN_POINT ( 'NONE',  ( -52.52205769399885327, -23.48786465467241058, 11.44779295918255357 ) ) ;
#9266=PLANE ( 'NONE',  #66395 ) ;
#9267=CARTESIAN_POINT ( 'NONE',  ( -50.52287095715006160, -23.47593901973090169, -1.443836447538997092 ) ) ;
#9268=CARTESIAN_POINT ( 'NONE',  ( 1.801620404824296084, -21.73869551012647605, -1.500000000000002220 ) ) ;
#9272=CARTESIAN_POINT ( 'NONE',  ( -48.95684766248727726, -25.26337410439581177, 6.634936722238220952 ) ) ;
#9273=ORIENTED_EDGE ( 'NONE', *, *, #28984, .F. ) ;
#9275=ORIENTED_EDGE ( 'NONE', *, *, #88865, .T. ) ;
#9278=CARTESIAN_POINT ( 'NONE',  ( -82.60434911312748341, -23.48783264082478084, -1.443836473390069264 ) ) ;
#9279=CARTESIAN_POINT ( 'NONE',  ( -20.47598858559898716, 5.595549388561865456, -1.500000000000002220 ) ) ;
#9280=CARTESIAN_POINT ( 'NONE',  ( -94.62287095715009855, -24.34917612406837861, 0.1852690917426660921 ) ) ;
#9281=CARTESIAN_POINT ( 'NONE',  ( -30.59755354180557418, -24.77158516743337913, 8.907023374642852431 ) ) ;
#9285=CARTESIAN_POINT ( 'NONE',  ( 12.26431755764203047, -15.03328313062362298, -1.500000000000002220 ) ) ;
#9287=CARTESIAN_POINT ( 'NONE',  ( -45.63257255548561631, -24.73486907724917572, 1.287355809206967017 ) ) ;
#9289=CARTESIAN_POINT ( 'NONE',  ( 0.4223197742854877812, 19.52780805513575402, 11.49999999999999645 ) ) ;
#9292=CARTESIAN_POINT ( 'NONE',  ( -108.6228709571500701, -23.73907113216991860, -1.053371485793227702 ) ) ;
#9297=CARTESIAN_POINT ( 'NONE',  ( -101.3313258111971749, -25.25498697735767095, 3.890283171256392780 ) ) ;
#9298=CARTESIAN_POINT ( 'NONE',  ( 10.71975780190685690, -16.47196428025586812, -1.500000000000002220 ) ) ;
#9300=CARTESIAN_POINT ( 'NONE',  ( 19.98343133220876666, -8.209121646405339590, -1.500000000000002220 ) ) ;
#9302=CARTESIAN_POINT ( 'NONE',  ( 22.28998074345494729, -6.091270044117925053, -1.500000000000002220 ) ) ;
#9303=EDGE_CURVE ( 'NONE', #11321, #46989, #49917, .T. ) ;
#9305=CARTESIAN_POINT ( 'NONE',  ( -91.62287095715004170, -23.47593901973091235, -1.443836447539002865 ) ) ;
#9306=FACE_OUTER_BOUND ( 'NONE', #23477, .T. ) ;
#9307=CARTESIAN_POINT ( 'NONE',  ( -76.52287095715009002, -23.73907113216989728, -1.053371485793248574 ) ) ;
#9309=CARTESIAN_POINT ( 'NONE',  ( -43.62287095715006302, -24.51387760970723662, 9.387446482453421837 ) ) ;
#9310=EDGE_CURVE ( 'NONE', #61298, #48580, #77408, .T. ) ;
#9311=CARTESIAN_POINT ( 'NONE',  ( -129.5895790072340219, -24.65952944569305316, 1.056160979905705677 ) ) ;
#9312=CARTESIAN_POINT ( 'NONE',  ( -114.5554595735986680, -23.96169478059714564, 10.65365249895717170 ) ) ;
#9313=CARTESIAN_POINT ( 'NONE',  ( 7.348632388941331861, 18.53259892055224611, -1.500000000000002220 ) ) ;
#9314=CARTESIAN_POINT ( 'NONE',  ( -75.51430423139920833, -23.85049219812685806, 10.88485053497527488 ) ) ;
#9316=CARTESIAN_POINT ( 'NONE',  ( 17.59243620335545799, -9.192777620008959261, -1.500000000000002220 ) ) ;
#9317=ORIENTED_EDGE ( 'NONE', *, *, #84311, .T. ) ;
#9320=CARTESIAN_POINT ( 'NONE',  ( -122.5228709571500616, -24.64965694238408034, 8.947790433994191162 ) ) ;
#9321=ADVANCED_FACE ( 'NONE', ( #8913 ), #38861, .T. ) ;
#9322=EDGE_CURVE ( 'NONE', #22334, #3335, #23120, .T. ) ;
#9323=CARTESIAN_POINT ( 'NONE',  ( -104.6228709571500559, -23.95044443724992078, 10.65354141964649592 ) ) ;
#9325=CARTESIAN_POINT ( 'NONE',  ( 12.91705851660734972, -16.24616318834520001, 11.49999999999999645 ) ) ;
#9328=CARTESIAN_POINT ( 'NONE',  ( -106.5533786925027329, -24.15543982623907482, -0.2315651400026576268 ) ) ;
#9329=CARTESIAN_POINT ( 'NONE',  ( -2.506051680461856890, -22.62920675306992280, 11.49999999999999645 ) ) ;
#9330=ORIENTED_EDGE ( 'NONE', *, *, #5221, .T. ) ;
#9331=B_SPLINE_SURFACE_WITH_KNOTS ( 'NONE', 3, 3, ( 
 ( #76976, #71392, #69381, #100301 ),
 ( #30818, #61783, #92703, #78477 ),
 ( #1384, #54177, #49061, #42947 ),
 ( #3391, #87102, #33819, #27214 ),
 ( #19585, #64298, #2889, #57670 ),
 ( #79492, #34825, #26710, #80996 ),
 ( #73883, #72394, #79989, #9979 ) ),
 .UNSPECIFIED., .F., .F., .F.,
 ( 4, 3, 4 ),
 ( 4, 4 ),
 ( 0.0004766839783834061822, 0.1029713700210900529, 0.2054660560637966982 ),
 ( 0.8697152379461190463, 0.8711292475148973979 ),
 .UNSPECIFIED. ) ;
#9333=CARTESIAN_POINT ( 'NONE',  ( -38.52287095715008292, -24.51283580621460345, 0.6167428607048118794 ) ) ;
#9334=ORIENTED_EDGE ( 'NONE', *, *, #46057, .F. ) ;
#9335=CARTESIAN_POINT ( 'NONE',  ( -17.47620107869530770, 10.18187089365592612, 11.49999999999998934 ) ) ;
#9337=EDGE_CURVE ( 'NONE', #44058, #87201, #76412, .T. ) ;
#9342=CARTESIAN_POINT ( 'NONE',  ( -127.5228709571500616, -24.65952944569304606, 1.056160979905707675 ) ) ;
#9343=CARTESIAN_POINT ( 'NONE',  ( -13.60431050971674694, 18.46711184989817411, 11.49999999999998934 ) ) ;
#9344=CARTESIAN_POINT ( 'NONE',  ( -51.62287095715005592, -24.65952944569304250, 1.056160979905695019 ) ) ;
#9345=CARTESIAN_POINT ( 'NONE',  ( -0.003041637939312698616, 19.98351707251910980, -1.500000000000002220 ) ) ;
#9346=CARTESIAN_POINT ( 'NONE',  ( -104.6228709571500985, -23.73907113216990794, -1.053371485793226814 ) ) ;
#9347=CARTESIAN_POINT ( 'NONE',  ( 8.737904895026865404, 19.08465823478955414, 11.49999999999999645 ) ) ;
#9348=DIRECTION ( 'NONE',  ( -3.773278334453079030E-23, 0.9999999999976377785, 2.173523156925979128E-06 ) ) ;
#9350=CARTESIAN_POINT ( 'NONE',  ( 1.153593019990587942, -22.03401787307112869, 11.49999999999998934 ) ) ;
#9351=EDGE_CURVE ( 'NONE', #76612, #35157, #295, .T. ) ;
#9353=CARTESIAN_POINT ( 'NONE',  ( -34.52287095715006160, -23.48783264083359867, -1.443836473376372442 ) ) ;
#9354=EDGE_LOOP ( 'NONE', ( #48961, #55318, #66099, #96426 ) ) ;
#9355=FACE_OUTER_BOUND ( 'NONE', #45570, .T. ) ;
#9356=CARTESIAN_POINT ( 'NONE',  ( -49.68454138742491466, -25.27344818403857474, 3.564592451155844000 ) ) ;
#9359=CARTESIAN_POINT ( 'NONE',  ( -47.52287095715006160, -24.64898659630528854, 1.056161002820821038 ) ) ;
#9362=ORIENTED_EDGE ( 'NONE', *, *, #29834, .F. ) ;
#9364=CARTESIAN_POINT ( 'NONE',  ( -100.8972602205940063, -25.10935818312838919, 2.905315788652750086 ) ) ;
#9366=CARTESIAN_POINT ( 'NONE',  ( -6.383830130275963910, 19.51498944528526991, -1.500000000000002220 ) ) ;
#9369=CARTESIAN_POINT ( 'NONE',  ( -61.55620429048339304, -23.47596703998600276, 11.44779298504227505 ) ) ;
#9370=CARTESIAN_POINT ( 'NONE',  ( -44.49316010094732832, -24.34968618360933590, 0.1864209137778786995 ) ) ;
#9372=CARTESIAN_POINT ( 'NONE',  ( -21.31523168734759466, -6.469442287714795015, 11.49999999999998934 ) ) ;
#9374=CARTESIAN_POINT ( 'NONE',  ( -0.1255922731526210312, -21.42410932854646433, 10.97511746239722363 ) ) ;
#9377=EDGE_CURVE ( 'NONE', #90387, #9703, #75409, .T. ) ;
#9379=CARTESIAN_POINT ( 'NONE',  ( -124.6228709571500559, -23.47593901973091235, -1.443836447538997536 ) ) ;
#9380=CARTESIAN_POINT ( 'NONE',  ( 18.58881047053902691, 9.431966241625852732, -1.500000000000002220 ) ) ;
#9381=EDGE_LOOP ( 'NONE', ( #99577, #98081, #93812, #94130 ) ) ;
#9383=ORIENTED_EDGE ( 'NONE', *, *, #73823, .F. ) ;
#9384=ORIENTED_EDGE ( 'NONE', *, *, #22098, .T. ) ;
#9385=DIRECTION ( 'NONE',  ( -3.773278334453080206E-23, 0.9999999999976377785, 2.173523156925979975E-06 ) ) ;
#9386=EDGE_CURVE ( 'NONE', #20637, #89121, #95904, .T. ) ;
#9387=CARTESIAN_POINT ( 'NONE',  ( 17.94697546605861760, -10.91086909363634838, -1.500000000000002220 ) ) ;
#9389=CARTESIAN_POINT ( 'NONE',  ( -36.62287095715005592, -23.47593901973091235, -1.443836447539011525 ) ) ;
#9393=CARTESIAN_POINT ( 'NONE',  ( -59.50898190215452388, -23.96119346886879597, -0.6495511937832131322 ) ) ;
#9394=LINE ( 'NONE', #92256, #85271 ) ;
#9395=CARTESIAN_POINT ( 'NONE',  ( -57.52287095715003318, -24.34917612406836440, 0.1852690917426539075 ) ) ;
#9396=CARTESIAN_POINT ( 'NONE',  ( 19.92104321119709098, 9.795001720801039369, 11.49999999999999645 ) ) ;
#9398=LINE ( 'NONE', #790, #66460 ) ;
#9399=CARTESIAN_POINT ( 'NONE',  ( -87.52287095715001897, -24.34917612407029353, 0.1852690917476594312 ) ) ;
#9400=VERTEX_POINT ( 'NONE', #85532 ) ;
#9401=CARTESIAN_POINT ( 'NONE',  ( -19.30582015231555104, -11.89196067722419237, 11.49999999999998934 ) ) ;
#9404=ORIENTED_EDGE ( 'NONE', *, *, #81843, .T. ) ;
#9407=CARTESIAN_POINT ( 'NONE',  ( 18.53703574427524359, 7.882278514257341051, -1.500000000000002220 ) ) ;
#9409=ORIENTED_EDGE ( 'NONE', *, *, #86216, .F. ) ;
#9410=CARTESIAN_POINT ( 'NONE',  ( -58.58953762381671737, -23.48783264082478439, -1.443836473390069264 ) ) ;
#9411=CARTESIAN_POINT ( 'NONE',  ( 20.99545381566289137, 7.807860396396394620, -1.500000000000002220 ) ) ;
#9412=ORIENTED_EDGE ( 'NONE', *, *, #51413, .F. ) ;
#9413=EDGE_LOOP ( 'NONE', ( #71384, #76610, #1249, #34376 ) ) ;
#9414=CARTESIAN_POINT ( 'NONE',  ( -112.5870093442895552, -24.66019654487200086, 8.947790411086112172 ) ) ;
#9415=CARTESIAN_POINT ( 'NONE',  ( -94.59719660544779174, -23.73791477778912196, 11.05961554403170588 ) ) ;
#9420=FACE_BOUND ( 'NONE', #42955, .T. ) ;
#9421=CARTESIAN_POINT ( 'NONE',  ( -18.58057592369839384, -6.135153870360039896, 11.49999999999998934 ) ) ;
#9424=CARTESIAN_POINT ( 'NONE',  ( 10.13398631766115443, 18.95262098133242290, 11.49999999999998934 ) ) ;
#9427=CARTESIAN_POINT ( 'NONE',  ( -123.5228709571500474, -24.51387760970726504, 9.387446482453404073 ) ) ;
#9428=PLANE ( 'NONE',  #19634 ) ;
#9429=CARTESIAN_POINT ( 'NONE',  ( 22.67525425759127344, 3.225002893152739247, -1.500000000000002220 ) ) ;
#9432=B_SPLINE_CURVE_WITH_KNOTS ( 'NONE', 3,
 ( #43249, #11286, #42266, #28015, #35132, #4682, #35631, #73198, #81298, #87915, #65104, #96519, #96023, #26519, #56979, #27015, #18398, #57982, #11782, #57482 ),
 .UNSPECIFIED., .F., .F.,
 ( 4, 2, 2, 2, 2, 2, 2, 2, 2, 4 ),
 ( 0.01762611779143858845, 0.01933231655155710771, 0.02018541593161636907, 0.02103851531167562697, 0.02274471407179414623, 0.02445091283191266548, 0.02786331035214970400, 0.02871640973220896190, 0.02956950911226821979, 0.03127570787238673905 ),
 .UNSPECIFIED. ) ;
#9434=CARTESIAN_POINT ( 'NONE',  ( -93.62287095715005592, -24.65952944569304606, 1.056160979905701236 ) ) ;
#9435=CARTESIAN_POINT ( 'NONE',  ( -70.48090377608006918, -25.31151630342660752, 5.317320600521428631 ) ) ;
#9436=CARTESIAN_POINT ( 'NONE',  ( 9.011679573027636891, 17.89655708981447901, 11.49999999999999645 ) ) ;
#9437=CARTESIAN_POINT ( 'NONE',  ( -80.30894842687054336, -25.26612373909271625, 4.506569033378546862 ) ) ;
#9439=EDGE_CURVE ( 'NONE', #18541, #91718, #54768, .T. ) ;
#9443=B_SPLINE_CURVE_WITH_KNOTS ( 'NONE', 3,
 ( #7778, #38224, #6775, #100099 ),
 .UNSPECIFIED., .F., .F.,
 ( 4, 4 ),
 ( 0.000000000000000000, 9.999999999997510880E-05 ),
 .UNSPECIFIED. ) ;
#9444=CARTESIAN_POINT ( 'NONE',  ( -39.52287095715006870, -23.47596703998600631, 11.44779298504229281 ) ) ;
#9445=CARTESIAN_POINT ( 'NONE',  ( -85.62287095715009855, -24.62226745350437440, 0.9660975649728092973 ) ) ;
#9447=CARTESIAN_POINT ( 'NONE',  ( -3.058130702743298901, -21.54894043062209263, -1.500000000000002220 ) ) ;
#9448=CARTESIAN_POINT ( 'NONE',  ( -90.62287095715002749, -25.00182538069145366, 7.747789668545099317 ) ) ;
#9449=CARTESIAN_POINT ( 'NONE',  ( 2.289404864003111051, -19.52285375609543294, -1.500000000000002220 ) ) ;
#9450=EDGE_CURVE ( 'NONE', #56961, #58188, #10413, .T. ) ;
#9452=EDGE_CURVE ( 'NONE', #91541, #87632, #31748, .T. ) ;
#9454=FACE_OUTER_BOUND ( 'NONE', #57114, .T. ) ;
#9456=CARTESIAN_POINT ( 'NONE',  ( -91.63120720951806675, -24.15620529776628445, 10.23563542870660115 ) ) ;
#9458=CARTESIAN_POINT ( 'NONE',  ( -10.41206725544052780, -17.73373708237225799, 11.49999999999999645 ) ) ;
#9459=PLANE ( 'NONE',  #78133 ) ;
#9460=CARTESIAN_POINT ( 'NONE',  ( -120.5884188931606644, -24.83618233451451118, 1.606449574219542598 ) ) ;
#9461=CARTESIAN_POINT ( 'NONE',  ( -22.56969522194696509, -0.6267768857631424995, 11.49999999999999645 ) ) ;
#9462=EDGE_LOOP ( 'NONE', ( #78487, #53291, #72691, #96306 ) ) ;
#9463=CARTESIAN_POINT ( 'NONE',  ( -70.12829555472771403, -25.25639598314597478, 7.087033306383300868 ) ) ;
#9464=CARTESIAN_POINT ( 'NONE',  ( -60.62287095715004881, -24.99132157543084531, 2.256160258750667502 ) ) ;
#9465=CARTESIAN_POINT ( 'NONE',  ( -51.23496102711971645, -25.29265441195226671, 4.254405096667612796 ) ) ;
#9466=CARTESIAN_POINT ( 'NONE',  ( -100.6814946224345846, -25.31267346029541443, 4.736250531364077254 ) ) ;
#9468=CARTESIAN_POINT ( 'NONE',  ( -117.6228709571500559, -23.47596703998600631, 11.44779298504227683 ) ) ;
#9471=EDGE_CURVE ( 'NONE', #55321, #21027, #88726, .T. ) ;
#9472=CARTESIAN_POINT ( 'NONE',  ( -80.19887417545862718, -25.26749879569623047, 4.982290670770169072 ) ) ;
#9473=CARTESIAN_POINT ( 'NONE',  ( -0.7673284989158746239, 22.82873350090251918, -1.500000000000002220 ) ) ;
#9474=CARTESIAN_POINT ( 'NONE',  ( -74.53891675414917017, -24.65952944569304606, 1.056160979905701902 ) ) ;
#9475=FACE_OUTER_BOUND ( 'NONE', #78929, .T. ) ;
#9476=CARTESIAN_POINT ( 'NONE',  ( -63.56611925033352151, -23.48786465467241058, 11.44779295918254824 ) ) ;
#9477=CARTESIAN_POINT ( 'NONE',  ( 12.99221220249228281, -18.32192329980629708, 11.49999999999999645 ) ) ;
#9478=ORIENTED_EDGE ( 'NONE', *, *, #62782, .T. ) ;
#9479=B_SPLINE_CURVE_WITH_KNOTS ( 'NONE', 3,
 ( #22361, #70060, #8667, #29991 ),
 .UNSPECIFIED., .F., .F.,
 ( 4, 4 ),
 ( 0.000000000000000000, 0.0001000000000000028644 ),
 .UNSPECIFIED. ) ;
#9480=CARTESIAN_POINT ( 'NONE',  ( -38.62287095715005592, -23.72773821059535848, 11.05748984161097503 ) ) ;
#9481=B_SPLINE_CURVE_WITH_KNOTS ( 'NONE', 3,
 ( #52872, #28521, #81818, #59484 ),
 .UNSPECIFIED., .F., .F.,
 ( 4, 4 ),
 ( 0.000000000000000000, 0.0001000000000000028644 ),
 .UNSPECIFIED. ) ;
#9482=CARTESIAN_POINT ( 'NONE',  ( 11.39931579351042679, 18.75040340349860557, -1.500000000000002220 ) ) ;
#9483=CARTESIAN_POINT ( 'NONE',  ( -124.6623340026854834, -25.38352273315424057, 4.245316684715575661 ) ) ;
#9484=CARTESIAN_POINT ( 'NONE',  ( -110.5562042904833788, -25.00158670708909625, 2.256160236439166855 ) ) ;
#9488=CARTESIAN_POINT ( 'NONE',  ( -97.52287095715007581, -23.47593901973090524, -1.443836447538996648 ) ) ;
#9490=CARTESIAN_POINT ( 'NONE',  ( -19.64171699416042571, -5.764624264842452384, -1.500000000000002220 ) ) ;
#9491=ORIENTED_EDGE ( 'NONE', *, *, #12082, .F. ) ;
#9492=EDGE_LOOP ( 'NONE', ( #30468, #28625, #63559, #55292 ) ) ;
#9493=ORIENTED_EDGE ( 'NONE', *, *, #82578, .F. ) ;
#9494=ORIENTED_EDGE ( 'NONE', *, *, #50856, .T. ) ;
#9495=CARTESIAN_POINT ( 'NONE',  ( -8.701767255460435280, 21.38705905713849020, 11.49999999999998934 ) ) ;
#9496=DIRECTION ( 'NONE',  ( -0.000000000000000000, 2.173523156925979552E-06, -0.9999999999976378895 ) ) ;
#9497=CARTESIAN_POINT ( 'NONE',  ( 6.837353022973060135, 19.10023500134885310, -1.500000000000002220 ) ) ;
#9498=ORIENTED_EDGE ( 'NONE', *, *, #4434, .T. ) ;
#9500=AXIS2_PLACEMENT_3D ( 'NONE', #91929, #7186, #91421 ) ;
#9505=CARTESIAN_POINT ( 'NONE',  ( -0.7226137440361984909, -21.50112622129444162, 11.49999999999999645 ) ) ;
#9506=ORIENTED_EDGE ( 'NONE', *, *, #54633, .T. ) ;
#9507=CARTESIAN_POINT ( 'NONE',  ( -89.55620429048337883, -24.64965694238574656, 8.947790433994201820 ) ) ;
#9508=CARTESIAN_POINT ( 'NONE',  ( -112.5228709571500616, -24.64898659630529210, 1.056161002820831474 ) ) ;
#9510=CARTESIAN_POINT ( 'NONE',  ( -11.67826063220891086, 17.12864047899337550, 11.49999999999998934 ) ) ;
#9512=ORIENTED_EDGE ( 'NONE', *, *, #31678, .F. ) ;
#9513=CARTESIAN_POINT ( 'NONE',  ( -125.6236348478159073, -24.92564183028979485, 1.928384488918254425 ) ) ;
#9515=CARTESIAN_POINT ( 'NONE',  ( -111.6245959756683561, -24.51419770103157703, 9.386484678747162747 ) ) ;
#9516=CARTESIAN_POINT ( 'NONE',  ( -53.52287095715006870, -24.65952944569304606, 1.056160979905693686 ) ) ;
#9517=VERTEX_POINT ( 'NONE', #71827 ) ;
#9518=ORIENTED_EDGE ( 'NONE', *, *, #43400, .T. ) ;
#9519=CARTESIAN_POINT ( 'NONE',  ( -109.5895376238167245, -23.47596703998600631, 11.44779298504227683 ) ) ;
#9520=AXIS2_PLACEMENT_3D ( 'NONE', #24060, #7841, #1245 ) ;
#9521=CARTESIAN_POINT ( 'NONE',  ( -42.65525658569841028, -23.73791477778911485, 11.05961554403171299 ) ) ;
#9522=CARTESIAN_POINT ( 'NONE',  ( -29.72012931874203900, -25.17545358843327108, 3.652302162786316142 ) ) ;
#9523=CARTESIAN_POINT ( 'NONE',  ( 8.687672273659204691, 20.25853876245846408, 11.49999999999999645 ) ) ;
#9525=CARTESIAN_POINT ( 'NONE',  ( -48.93017815765824707, -25.21617556241885438, 6.556673522205215932 ) ) ;
#9526=CARTESIAN_POINT ( 'NONE',  ( 10.27952223434480494, 20.12118371629609470, 11.49999999999998934 ) ) ;
#9527=B_SPLINE_CURVE_WITH_KNOTS ( 'NONE', 3,
 ( #8854, #21202, #44557, #1257, #32186, #98828 ),
 .UNSPECIFIED., .F., .F.,
 ( 4, 2, 4 ),
 ( 0.000000000000000000, 0.001380901958385387894, 0.002761803916770775788 ),
 .UNSPECIFIED. ) ;
#9528=CARTESIAN_POINT ( 'NONE',  ( 18.89479412359299815, 9.153864009170110450, -1.500000000000002220 ) ) ;
#9529=FACE_OUTER_BOUND ( 'NONE', #62430, .T. ) ;
#9531=B_SPLINE_CURVE_WITH_KNOTS ( 'NONE', 3,
 ( #41447, #85737, #2899, #72405 ),
 .UNSPECIFIED., .F., .F.,
 ( 4, 4 ),
 ( 0.6109362546251637660, 0.6199426858972792997 ),
 .UNSPECIFIED. ) ;
#9532=ORIENTED_EDGE ( 'NONE', *, *, #95831, .F. ) ;
#9535=ORIENTED_EDGE ( 'NONE', *, *, #17582, .T. ) ;
#9536=CARTESIAN_POINT ( 'NONE',  ( 10.98566517548414012, -18.08203305749968592, -1.500000000000002220 ) ) ;
#9537=DIRECTION ( 'NONE',  ( 1.000000000000000000, 3.773278334444166432E-23, 8.201307841325785021E-29 ) ) ;
#9538=CARTESIAN_POINT ( 'NONE',  ( -59.79220569025929422, -25.27183489919805126, 3.712349809207164952 ) ) ;
#9539=CARTESIAN_POINT ( 'NONE',  ( -75.62287095715005592, -23.47593901973091235, -1.443836447539004642 ) ) ;
#9540=CARTESIAN_POINT ( 'NONE',  ( -32.55620429048339304, -23.47596703998600276, 11.44779298504227505 ) ) ;
#9542=CARTESIAN_POINT ( 'NONE',  ( 22.20168578472828358, 1.497490109320031682, -1.500000000000002220 ) ) ;
#9543=CARTESIAN_POINT ( 'NONE',  ( -49.72218425784361528, -25.03220880655923608, 7.443037874571290402 ) ) ;
#9544=ORIENTED_EDGE ( 'NONE', *, *, #58941, .F. ) ;
#9546=CARTESIAN_POINT ( 'NONE',  ( -37.49079198358890608, -24.34968618360933590, 0.1864209137778856384 ) ) ;
#9548=CARTESIAN_POINT ( 'NONE',  ( -100.5484642610753951, -24.63355581998385091, 0.9682620441943978751 ) ) ;
#9550=CARTESIAN_POINT ( 'NONE',  ( 6.171429453590791425, 18.48145409631445446, -1.500000000000002220 ) ) ;
#9551=CARTESIAN_POINT ( 'NONE',  ( 21.20698605602738951, -2.876969938318672870, -1.500000000000002220 ) ) ;
#9553=CARTESIAN_POINT ( 'NONE',  ( -60.48076987232976620, -25.00182538069856619, 7.747789668514392325 ) ) ;
#9554=CARTESIAN_POINT ( 'NONE',  ( -100.6228709571500559, -25.00182538069145721, 7.747789668545099317 ) ) ;
#9555=CARTESIAN_POINT ( 'NONE',  ( -100.8624150394625616, -25.18440029588451168, 3.378658976843279760 ) ) ;
#9556=CARTESIAN_POINT ( 'NONE',  ( -17.51746294255814718, -14.55262482891283504, -1.500000000000002220 ) ) ;
#9558=CARTESIAN_POINT ( 'NONE',  ( -102.5888672789946980, -24.34968618360934656, 0.1864209137778959358 ) ) ;
#9559=CARTESIAN_POINT ( 'NONE',  ( -98.62287095715005592, -23.96127896941632685, -0.6493128931037821516 ) ) ;
#9560=CARTESIAN_POINT ( 'NONE',  ( 16.83370257367741019, -10.51912618480096206, 11.49999999999999645 ) ) ;
#9562=AXIS2_PLACEMENT_3D ( 'NONE', #14078, #36427, #12084 ) ;
#9563=EDGE_CURVE ( 'NONE', #19646, #908, #91042, .T. ) ;
#9564=AXIS2_PLACEMENT_3D ( 'NONE', #33695, #16448, #8847 ) ;
#9565=FACE_OUTER_BOUND ( 'NONE', #93133, .T. ) ;
#9566=CARTESIAN_POINT ( 'NONE',  ( -65.52287095715006160, -23.47593901973090169, -1.443836447538996870 ) ) ;
#9567=ORIENTED_EDGE ( 'NONE', *, *, #87451, .T. ) ;
#9568=CARTESIAN_POINT ( 'NONE',  ( -49.86628797114703815, -25.13894531369371421, 7.008864803050190773 ) ) ;
#9571=CARTESIAN_POINT ( 'NONE',  ( -50.89113880358890185, -25.27412246153383890, 2.917241017069057030 ) ) ;
#9572=CARTESIAN_POINT ( 'NONE',  ( -21.36891742734480104, 3.643610035731704055, 11.49999999999998934 ) ) ;
#9573=CARTESIAN_POINT ( 'NONE',  ( -56.55997175465316218, -23.73791477778911840, 11.05961554403170766 ) ) ;
#9575=CARTESIAN_POINT ( 'NONE',  ( -15.31790942089943286, 12.02624123284522106, -1.500000000000002220 ) ) ;
#9576=EDGE_CURVE ( 'NONE', #64433, #72799, #56023, .T. ) ;
#9577=FACE_OUTER_BOUND ( 'NONE', #14020, .T. ) ;
#9579=EDGE_CURVE ( 'NONE', #5085, #46960, #85120, .T. ) ;
#9581=CARTESIAN_POINT ( 'NONE',  ( 3.609400094169940676, -20.08663944828865766, 11.49999999999999645 ) ) ;
#9582=LINE ( 'NONE', #78572, #86126 ) ;
#9584=B_SPLINE_CURVE_WITH_KNOTS ( 'NONE', 3,
 ( #71124, #86834, #17325, #100035 ),
 .UNSPECIFIED., .F., .F.,
 ( 4, 4 ),
 ( 0.000000000000000000, 9.999999999998897304E-05 ),
 .UNSPECIFIED. ) ;
#9587=CARTESIAN_POINT ( 'NONE',  ( -80.09320475646708815, -25.04201173125214908, 7.520314828238249483 ) ) ;
#9589=CARTESIAN_POINT ( 'NONE',  ( -39.36780865613509661, -25.27985487685322141, 5.233841631192319710 ) ) ;
#9591=CARTESIAN_POINT ( 'NONE',  ( -49.32129151558435609, -25.31439425002071530, 5.877610906657145584 ) ) ;
#9593=CARTESIAN_POINT ( 'NONE',  ( 18.22116949570664701, -8.484823103377051368, -1.500000000000002220 ) ) ;
#9595=ORIENTED_EDGE ( 'NONE', *, *, #80933, .T. ) ;
#9597=CARTESIAN_POINT ( 'NONE',  ( -13.60431050971674694, 18.46711184989817411, 11.49999999999999645 ) ) ;
#9598=CARTESIAN_POINT ( 'NONE',  ( 18.51665531608540860, 13.21585733361752801, -1.500000000000002220 ) ) ;
#9600=CARTESIAN_POINT ( 'NONE',  ( -30.47287095715005734, -25.21920238677788362, 6.407047544386642812 ) ) ;
#9601=CARTESIAN_POINT ( 'NONE',  ( -98.52287095715006160, -24.65952944569304606, 1.056160979905702346 ) ) ;
#9602=CARTESIAN_POINT ( 'NONE',  ( -81.52287095715006160, -24.64965694238408034, 8.947790433994198267 ) ) ;
#9603=CARTESIAN_POINT ( 'NONE',  ( -30.57287095715006942, -23.48213395187224606, 11.44779283644488999 ) ) ;
#9604=CARTESIAN_POINT ( 'NONE',  ( -69.51084105356602549, -23.96169478059712787, 10.65365249895718414 ) ) ;
#9605=AXIS2_PLACEMENT_3D ( 'NONE', #44775, #37650, #98038 ) ;
#9606=CARTESIAN_POINT ( 'NONE',  ( -27.68651082257923335, -24.77145582263907286, 2.274903367125437281 ) ) ;
#9608=CARTESIAN_POINT ( 'NONE',  ( -99.04404089887771079, -25.25460591887426531, 5.494369256536408841 ) ) ;
#9610=CARTESIAN_POINT ( 'NONE',  ( 20.11976772532220181, -3.360927329567881205, 11.49999999999998934 ) ) ;
#9611=EDGE_LOOP ( 'NONE', ( #52192, #66396, #80001, #91808, #67147, #71073, #85023, #2644 ) ) ;
#9612=ORIENTED_EDGE ( 'NONE', *, *, #83269, .T. ) ;
#9613=CARTESIAN_POINT ( 'NONE',  ( -6.685540227124203483, -22.02754839873749404, -1.500000000000002220 ) ) ;
#9616=PLANE ( 'NONE',  #44454 ) ;
#9618=B_SPLINE_CURVE_WITH_KNOTS ( 'NONE', 3,
 ( #66870, #58744, #59247, #3473, #49647, #20169, #82078, #12562, #43526, #74463, #90188, #13052, #7438, #59753, #29785, #98282, #30785, #6945, #44013, #60751, #36401, #100266 ),
 .UNSPECIFIED., .F., .F.,
 ( 4, 2, 2, 2, 2, 2, 2, 2, 2, 2, 4 ),
 ( 8.673617379884035472E-19, 0.0005541007949657107429, 0.001108201589931420619, 0.001662302384897130711, 0.002216403179862840370, 0.002770503974828550462, 0.003047554372311408761, 0.003324604769794267060, 0.003878705564759983224, 0.004155755962242840655, 0.004432806359725698954 ),
 .UNSPECIFIED. ) ;
#9619=CARTESIAN_POINT ( 'NONE',  ( -95.63923414667179657, -23.85016227208581086, -0.8807180028928282001 ) ) ;
#9620=CARTESIAN_POINT ( 'NONE',  ( -119.4728709571500360, -25.30558663486607429, 5.000950657679038791 ) ) ;
#9621=CARTESIAN_POINT ( 'NONE',  ( -6.196366259867160942, 20.41550611124569059, 11.49999999999999645 ) ) ;
#9622=ORIENTED_EDGE ( 'NONE', *, *, #94115, .F. ) ;
#9623=ORIENTED_EDGE ( 'NONE', *, *, #76817, .F. ) ;
#9624=CARTESIAN_POINT ( 'NONE',  ( -21.66996937300057269, -4.939502015459471096, 11.49999999999998934 ) ) ;
#9625=CARTESIAN_POINT ( 'NONE',  ( 17.37421522561336928, 11.14841987994331696, 11.49999999999998934 ) ) ;
#9626=EDGE_CURVE ( 'NONE', #44485, #16795, #70566, .T. ) ;
#9627=ORIENTED_EDGE ( 'NONE', *, *, #29992, .F. ) ;
#9630=CARTESIAN_POINT ( 'NONE',  ( -95.51302621525215386, -24.15602025860896163, 10.28564288303535967 ) ) ;
#9631=ORIENTED_EDGE ( 'NONE', *, *, #43474, .T. ) ;
#9632=CARTESIAN_POINT ( 'NONE',  ( -124.5228709571500616, -29.50250786944525672, 11.44777988621622811 ) ) ;
#9638=CARTESIAN_POINT ( 'NONE',  ( -13.77211689728001964, -15.67653869864640903, -1.500000000000002220 ) ) ;
#9639=CARTESIAN_POINT ( 'NONE',  ( -19.95566455537076678, 8.849265345510103131, 11.49999999999999645 ) ) ;
#9641=CARTESIAN_POINT ( 'NONE',  ( -37.62287095715005592, -23.48783264082477373, -1.443836473390072372 ) ) ;
#9642=CARTESIAN_POINT ( 'NONE',  ( 20.54305097139451064, 9.177977666691313985, -1.500000000000002220 ) ) ;
#9644=DIRECTION ( 'NONE',  ( 0.000000000000000000, 0.9999999999976377785, 2.173523156925979975E-06 ) ) ;
#9646=CARTESIAN_POINT ( 'NONE',  ( -54.55620429048340014, -24.65952944569304606, 1.056160979905694131 ) ) ;
#9650=AXIS2_PLACEMENT_3D ( 'NONE', #17842, #71631, #87339 ) ;
#9651=ORIENTED_EDGE ( 'NONE', *, *, #13084, .F. ) ;
#9652=CARTESIAN_POINT ( 'NONE',  ( -100.3181550757389147, -25.26221317742673378, 7.099294928845378827 ) ) ;
#9653=EDGE_CURVE ( 'NONE', #88472, #43961, #68205, .T. ) ;
#9655=VECTOR ( 'NONE', #85898, 1000.000000000000114 ) ;
#9656=CARTESIAN_POINT ( 'NONE',  ( 21.39645853268639186, 0.3907444525687319703, -1.500000000000002220 ) ) ;
#9657=CARTESIAN_POINT ( 'NONE',  ( 20.23429811176546167, 9.490607074118958764, 11.49999999999999645 ) ) ;
#9658=ORIENTED_EDGE ( 'NONE', *, *, #17709, .F. ) ;
#9660=CARTESIAN_POINT ( 'NONE',  ( 20.41947327098772647, -5.118016103960565388, -1.500000000000002220 ) ) ;
#9661=CARTESIAN_POINT ( 'NONE',  ( -30.44997090143552043, -24.04449549154637111, 10.47557002954947336 ) ) ;
#9662=CARTESIAN_POINT ( 'NONE',  ( 1.593314845114734535, -19.89410510517485164, -1.500000000000002220 ) ) ;
#9665=CARTESIAN_POINT ( 'NONE',  ( -114.5562042904833930, -23.48786465467241769, 11.44779295918253936 ) ) ;
#9666=CARTESIAN_POINT ( 'NONE',  ( -64.62287095715005592, -24.65952944569304250, 1.056160979905695685 ) ) ;
#9667=CARTESIAN_POINT ( 'NONE',  ( -15.57331531552114612, -15.56871402003811333, -1.500000000000002220 ) ) ;
#9668=ORIENTED_EDGE ( 'NONE', *, *, #12309, .T. ) ;
#9669=CARTESIAN_POINT ( 'NONE',  ( -65.49580353523785448, -24.52399227489126687, 9.353111116836529959 ) ) ;
#9670=CARTESIAN_POINT ( 'NONE',  ( -64.62287095715005592, -29.50250243563736774, 8.947779886222145151 ) ) ;
#9671=CARTESIAN_POINT ( 'NONE',  ( -19.30504728598367237, -7.930543132070424051, 11.49999999999999645 ) ) ;
#9673=CARTESIAN_POINT ( 'NONE',  ( -125.5228709571500616, -24.82576562948885623, 8.398263436605594379 ) ) ;
#9675=CARTESIAN_POINT ( 'NONE',  ( -19.36244235409943926, 8.944087295975924334, -1.500000000000002220 ) ) ;
#9676=DIRECTION ( 'NONE',  ( 3.773278334444167608E-23, -1.000000000000000000, 0.000000000000000000 ) ) ;
#9678=CARTESIAN_POINT ( 'NONE',  ( -75.62287095715005592, -23.48783264082478084, -1.443836473390065489 ) ) ;
#9680=CARTESIAN_POINT ( 'NONE',  ( -10.21242994381667657, -20.12718729479640700, -1.500000000000002220 ) ) ;
#9683=CARTESIAN_POINT ( 'NONE',  ( -79.98140449170570321, -25.29705034626280025, 4.546672010081276305 ) ) ;
#9685=CARTESIAN_POINT ( 'NONE',  ( -15.16924259816527609, 12.53091941037558854, 11.49999999999999645 ) ) ;
#9690=CARTESIAN_POINT ( 'NONE',  ( -55.62287095715005592, -23.47593901973091235, -1.443836447539007972 ) ) ;
#9693=CARTESIAN_POINT ( 'NONE',  ( -95.52287095715011844, -24.83620972994591725, 8.398175272781369216 ) ) ;
#9695=CARTESIAN_POINT ( 'NONE',  ( -126.5228709571500616, -29.50250243563736774, 8.947779886222132717 ) ) ;
#9696=CARTESIAN_POINT ( 'NONE',  ( 18.24634267693259559, -7.554628487255452107, -1.500000000000002220 ) ) ;
#9697=EDGE_LOOP ( 'NONE', ( #80618, #97957, #37094, #4192 ) ) ;
#9699=CARTESIAN_POINT ( 'NONE',  ( -16.41926757845921614, -11.79510067912178606, 11.49999999999999645 ) ) ;
#9701=EDGE_CURVE ( 'NONE', #38179, #5224, #23083, .T. ) ;
#9703=VERTEX_POINT ( 'NONE', #42881 ) ;
#9704=CARTESIAN_POINT ( 'NONE',  ( -117.6228709571500559, -29.50247984919015209, -1.443849546365046699 ) ) ;
#9706=CARTESIAN_POINT ( 'NONE',  ( -68.62287095715005592, -23.47593901973091235, -1.443836447539006196 ) ) ;
#9707=CARTESIAN_POINT ( 'NONE',  ( -83.22287095715010707, -23.47593901973090524, -1.443836447538997536 ) ) ;
#9710=LINE ( 'NONE', #79714, #98049 ) ;
#9711=CARTESIAN_POINT ( 'NONE',  ( -20.00956492049148494, -0.6725752471728385640, 11.49999999999998934 ) ) ;
#9712=ADVANCED_FACE ( 'NONE', ( #81927 ), #27651, .T. ) ;
#9713=CARTESIAN_POINT ( 'NONE',  ( -62.62287095715004881, -23.47593901973091235, -1.443836447539007972 ) ) ;
#9714=CARTESIAN_POINT ( 'NONE',  ( -116.5555263298079183, -23.96169478059713853, 10.65365249895717348 ) ) ;
#9716=AXIS2_PLACEMENT_3D ( 'NONE', #98364, #35977, #20741 ) ;
#9717=VECTOR ( 'NONE', #34214, 1000.000000000000114 ) ;
#9719=DIRECTION ( 'NONE',  ( -3.773278334444167608E-23, 1.000000000000000000, 0.000000000000000000 ) ) ;
#9720=CARTESIAN_POINT ( 'NONE',  ( -79.37567067213733196, -25.28636030991100370, 5.689218636705552612 ) ) ;
#9721=AXIS2_PLACEMENT_3D ( 'NONE', #53283, #51278, #83718 ) ;
#9722=CARTESIAN_POINT ( 'NONE',  ( -124.5228709571500616, -24.65952944569305316, 1.056160979905705899 ) ) ;
#9723=CARTESIAN_POINT ( 'NONE',  ( -83.64499529382760556, -23.48783264082477018, -1.443836473390093911 ) ) ;
#9726=LINE ( 'NONE', #55917, #97150 ) ;
#9727=EDGE_LOOP ( 'NONE', ( #14667, #88221, #87997, #44930 ) ) ;
#9728=CARTESIAN_POINT ( 'NONE',  ( 13.48481281434462531, 15.16087405922196041, 11.49999999999998934 ) ) ;
#9730=CARTESIAN_POINT ( 'NONE',  ( -34.52672225899539171, -24.65952944569304606, 1.056160979905694353 ) ) ;
#9731=CARTESIAN_POINT ( 'NONE',  ( -107.5228709571501184, -23.96177878511309345, 10.65340807706329507 ) ) ;
#9732=EDGE_LOOP ( 'NONE', ( #86978, #2511, #25124, #92848 ) ) ;
#9733=CARTESIAN_POINT ( 'NONE',  ( -81.62287095715008434, -24.34917612406837506, 0.1852690917426648154 ) ) ;
#9735=CARTESIAN_POINT ( 'NONE',  ( -12.03079493616482765, -17.41531974249929249, 11.49999999999999645 ) ) ;
#9736=CARTESIAN_POINT ( 'NONE',  ( 13.35222405703702186, 17.66689192352044913, 11.49999999999998934 ) ) ;
#9737=EDGE_CURVE ( 'NONE', #70011, #9517, #71640, .T. ) ;
#9738=CARTESIAN_POINT ( 'NONE',  ( 0.1292827521129817636, -20.55975067039486603, 11.49999999999998934 ) ) ;
#9739=VERTEX_POINT ( 'NONE', #52483 ) ;
#9740=CARTESIAN_POINT ( 'NONE',  ( -116.6228709571500559, -24.64965695001469115, 8.947790433994175174 ) ) ;
#9741=EDGE_LOOP ( 'NONE', ( #41238, #56920, #92463, #55551 ) ) ;
#9743=CARTESIAN_POINT ( 'NONE',  ( -110.6228709571500417, -24.15516710230295772, 10.28746687063727094 ) ) ;
#9750=CARTESIAN_POINT ( 'NONE',  ( -9.011640028862021978, 18.61544202926687674, -1.500000000000002220 ) ) ;
#9751=CARTESIAN_POINT ( 'NONE',  ( 21.02075834227166951, -5.193550065563941942, 11.49999999999999645 ) ) ;
#9755=CARTESIAN_POINT ( 'NONE',  ( 19.55810785529653373, 10.91776788121007868, 11.49999999999998934 ) ) ;
#9756=LINE ( 'NONE', #26988, #75590 ) ;
#9757=CARTESIAN_POINT ( 'NONE',  ( -84.58278115369181194, -24.65952944569303895, 1.056160979905700348 ) ) ;
#9760=DIRECTION ( 'NONE',  ( -3.773278334453079030E-23, 0.9999999999976377785, 2.173523156925979128E-06 ) ) ;
#9761=ORIENTED_EDGE ( 'NONE', *, *, #30298, .T. ) ;
#9764=DIRECTION ( 'NONE',  ( 3.773278334444167608E-23, -1.000000000000000000, 0.000000000000000000 ) ) ;
#9766=ORIENTED_EDGE ( 'NONE', *, *, #77825, .T. ) ;
#9767=DIRECTION ( 'NONE',  ( 2.145277261456712182E-39, 2.173523156925979128E-06, -0.9999999999976378895 ) ) ;
#9768=CARTESIAN_POINT ( 'NONE',  ( -14.73150212448299357, 15.28860238833873808, -1.500000000000002220 ) ) ;
#9770=CARTESIAN_POINT ( 'NONE',  ( -50.48629971621463142, -24.63355581998386867, 0.9682620441943859957 ) ) ;
#9771=CARTESIAN_POINT ( 'NONE',  ( 15.22768361601695020, -15.61070304372801587, 11.49999999999998934 ) ) ;
#9772=CARTESIAN_POINT ( 'NONE',  ( -103.5953284589405143, -23.73791477778911840, 11.05961554403170410 ) ) ;
#9775=CARTESIAN_POINT ( 'NONE',  ( 13.86046232669119149, 16.88393516940953276, -1.500000000000002220 ) ) ;
#9776=CARTESIAN_POINT ( 'NONE',  ( -30.57287095715004455, -25.10844925379378623, 7.250334085407572182 ) ) ;
#9777=ORIENTED_EDGE ( 'NONE', *, *, #43739, .F. ) ;
#9780=ORIENTED_EDGE ( 'NONE', *, *, #36647, .T. ) ;
#9781=EDGE_CURVE ( 'NONE', #1208, #25123, #65553, .T. ) ;
#9783=B_SPLINE_CURVE_WITH_KNOTS ( 'NONE', 3,
 ( #71343, #10941, #80952, #32769 ),
 .UNSPECIFIED., .F., .F.,
 ( 4, 4 ),
 ( 0.000000000000000000, 9.999999999998897304E-05 ),
 .UNSPECIFIED. ) ;
#9786=CARTESIAN_POINT ( 'NONE',  ( -89.49044894935767047, -25.12049752546738191, 2.832404795212222659 ) ) ;
#9788=CARTESIAN_POINT ( 'NONE',  ( -82.54408211365957015, -24.51314013834315375, 0.6176544820404155089 ) ) ;
#9789=CARTESIAN_POINT ( 'NONE',  ( -21.08860491664495029, 2.407354197416772035, 11.49999999999998934 ) ) ;
#9791=CARTESIAN_POINT ( 'NONE',  ( -30.61333094834725088, -24.36247485673954927, 0.01136689895587368430 ) ) ;
#9792=CARTESIAN_POINT ( 'NONE',  ( -73.62287095715005592, -29.50248528299804818, 1.056150453629036701 ) ) ;
#9793=FACE_OUTER_BOUND ( 'NONE', #82030, .T. ) ;
#9795=CARTESIAN_POINT ( 'NONE',  ( 15.36829964806744364, -11.83880051060199712, -1.500000000000002220 ) ) ;
#9796=CARTESIAN_POINT ( 'NONE',  ( -45.57860970357442909, -24.83618233451450408, 1.606449574219532384 ) ) ;
#9799=CARTESIAN_POINT ( 'NONE',  ( -19.43040671759091609, -1.856541507571394467, 11.49999999999999645 ) ) ;
#9802=CARTESIAN_POINT ( 'NONE',  ( -68.52287095715009002, -23.72747288104470087, -1.053458166803227014 ) ) ;
#9803=ORIENTED_EDGE ( 'NONE', *, *, #76050, .F. ) ;
#9805=CARTESIAN_POINT ( 'NONE',  ( -89.55462902144884652, -23.96119346886881374, -0.6495511937831908167 ) ) ;
#9806=CARTESIAN_POINT ( 'NONE',  ( -98.52287095715006160, -24.65952944569304606, 1.056160979905702346 ) ) ;
#9807=B_SPLINE_CURVE_WITH_KNOTS ( 'NONE', 3,
 ( #72592, #55874, #57383, #65000 ),
 .UNSPECIFIED., .F., .F.,
 ( 4, 4 ),
 ( 0.000000000000000000, 1.000000000000000000 ),
 .UNSPECIFIED. ) ;
#9808=CARTESIAN_POINT ( 'NONE',  ( -81.83126432988071031, -25.03155843045780315, 6.560967614844648743 ) ) ;
#9809=CARTESIAN_POINT ( 'NONE',  ( -18.24527198174902765, 7.358211898524878336, -1.500000000000002220 ) ) ;
#9812=CARTESIAN_POINT ( 'NONE',  ( -55.62287095715005592, -29.50248528299804818, 1.056150453629034924 ) ) ;
#9813=CARTESIAN_POINT ( 'NONE',  ( -43.52287095715006160, -24.64898659630528854, 1.056161002820819261 ) ) ;
#9814=EDGE_CURVE ( 'NONE', #65965, #8482, #81345, .T. ) ;
#9817=CARTESIAN_POINT ( 'NONE',  ( -90.52287095715003318, -24.62285846331438321, 9.038163153548227413 ) ) ;
#9818=CARTESIAN_POINT ( 'NONE',  ( -109.2887704616800590, -25.18211350563075257, 3.273023101274771918 ) ) ;
#9819=CARTESIAN_POINT ( 'NONE',  ( -97.52218080935233502, -23.48786465467241413, 11.44779295918254469 ) ) ;
#9822=CARTESIAN_POINT ( 'NONE',  ( -121.6228709571500843, -24.51387760970725083, 9.387446482453405849 ) ) ;
#9823=CARTESIAN_POINT ( 'NONE',  ( -111.3776484685884327, -25.18425808373743635, 4.332404656630714612 ) ) ;
#9824=CARTESIAN_POINT ( 'NONE',  ( -10.02925392579303576, -17.20239368982820238, -1.500000000000002220 ) ) ;
#9825=EDGE_CURVE ( 'NONE', #73894, #95505, #88542, .T. ) ;
#9826=CARTESIAN_POINT ( 'NONE',  ( -75.63385634215764242, -24.52399227489127043, 9.353111116836526406 ) ) ;
#9827=CARTESIAN_POINT ( 'NONE',  ( -9.134819693115781902, 17.59984377705169933, -1.500000000000002220 ) ) ;
#9830=CARTESIAN_POINT ( 'NONE',  ( -101.6228709571500559, -29.50248528299804818, 1.056150453629042030 ) ) ;
#9832=CARTESIAN_POINT ( 'NONE',  ( 2.040502595053849788, 20.68626321094233944, 11.49999999999999645 ) ) ;
#9835=CARTESIAN_POINT ( 'NONE',  ( -106.5926168708341635, -23.96119346886880308, -0.6495511937832030291 ) ) ;
#9836=CARTESIAN_POINT ( 'NONE',  ( -13.73562189146022661, -18.16285900770654393, 11.49999999999999645 ) ) ;
#9839=CARTESIAN_POINT ( 'NONE',  ( -100.6228709571500559, -25.00158670708909625, 2.256160236439166411 ) ) ;
#9840=ORIENTED_EDGE ( 'NONE', *, *, #43489, .T. ) ;
#9841=CARTESIAN_POINT ( 'NONE',  ( 14.71488472389458124, -13.84269218943631508, -1.500000000000002220 ) ) ;
#9842=FACE_OUTER_BOUND ( 'NONE', #99215, .T. ) ;
#9843=CARTESIAN_POINT ( 'NONE',  ( -69.55620429048339304, -23.48783264082478084, -1.443836473390067265 ) ) ;
#9844=ORIENTED_EDGE ( 'NONE', *, *, #67711, .F. ) ;
#9848=CARTESIAN_POINT ( 'NONE',  ( -11.50144725928494438, 16.33591932373696665, -1.500000000000002220 ) ) ;
#9850=CARTESIAN_POINT ( 'NONE',  ( 13.87900837158347755, -15.70065903812341013, 11.49999999999999645 ) ) ;
#9852=CARTESIAN_POINT ( 'NONE',  ( -106.5228709571500758, -24.64898659630368627, 1.056161002820831474 ) ) ;
#9853=CARTESIAN_POINT ( 'NONE',  ( -93.52287095715007581, -23.96177878511308990, 10.65340807706329684 ) ) ;
#9854=CARTESIAN_POINT ( 'NONE',  ( 9.306852550357104903, -20.00191182576189064, -1.500000000000002220 ) ) ;
#9855=B_SPLINE_CURVE_WITH_KNOTS ( 'NONE', 3,
 ( #4278, #17997, #49465, #18493 ),
 .UNSPECIFIED., .F., .F.,
 ( 4, 4 ),
 ( 0.000000000000000000, 9.999999999998897304E-05 ),
 .UNSPECIFIED. ) ;
#9856=B_SPLINE_CURVE_WITH_KNOTS ( 'NONE', 3,
 ( #34384, #87165, #26268, #11046, #65361, #96280, #79046, #40501 ),
 .UNSPECIFIED., .F., .F.,
 ( 4, 2, 2, 4 ),
 ( 0.000000000000000000, 0.002001098010032682784, 0.003001647015049024175, 0.004002196020065365567 ),
 .UNSPECIFIED. ) ;
#9857=CARTESIAN_POINT ( 'NONE',  ( -124.4728709548940486, -25.21112548385455199, 2.000950967214091936 ) ) ;
#9858=ADVANCED_FACE ( 'NONE', ( #22997, #46358 ), #82959, .T. ) ;
#9860=CARTESIAN_POINT ( 'NONE',  ( -127.6228709571500275, -23.48786465467242124, 11.44779295918253403 ) ) ;
#9861=CARTESIAN_POINT ( 'NONE',  ( -118.5228709571501184, -23.96177878511310055, 10.65340807706329507 ) ) ;
#9862=CARTESIAN_POINT ( 'NONE',  ( -72.63936276973265649, -23.96119346886880663, -0.6495511937832119109 ) ) ;
#9863=ORIENTED_EDGE ( 'NONE', *, *, #52297, .F. ) ;
#9866=ORIENTED_EDGE ( 'NONE', *, *, #38979, .T. ) ;
#9867=CARTESIAN_POINT ( 'NONE',  ( -101.7776484685884242, -25.26303730729093644, 3.986250639247583827 ) ) ;
#9870=CARTESIAN_POINT ( 'NONE',  ( -19.38928925021375349, 6.733644070511561885, -1.500000000000002220 ) ) ;
#9872=DIRECTION ( 'NONE',  ( -3.773278334453079618E-23, 0.9999999999976377785, 2.173523156925979975E-06 ) ) ;
#9875=CARTESIAN_POINT ( 'NONE',  ( -6.278373996654322831, -21.41630973362384083, -1.500000000000002220 ) ) ;
#9876=CARTESIAN_POINT ( 'NONE',  ( -90.62287095715004170, -23.47593901973091235, -1.443836447539002865 ) ) ;
#9881=CARTESIAN_POINT ( 'NONE',  ( -5.376107494350208960, -20.15860285114975525, 11.49999999999998934 ) ) ;
#9883=CARTESIAN_POINT ( 'NONE',  ( -79.52287095715007581, -24.35013146730203815, 9.818937971375103047 ) ) ;
#9884=ORIENTED_EDGE ( 'NONE', *, *, #11963, .F. ) ;
#9885=ADVANCED_FACE ( 'NONE', ( #32127 ), #85454, .T. ) ;
#9887=CARTESIAN_POINT ( 'NONE',  ( -70.15801421577009478, -25.25935349274321950, 7.556454315002589794 ) ) ;
#9888=CARTESIAN_POINT ( 'NONE',  ( 11.68726034403320746, 17.49698133428071145, -1.500000000000002220 ) ) ;
#9890=CARTESIAN_POINT ( 'NONE',  ( -110.6228709571500559, -29.50248789122583659, 2.256150453626215580 ) ) ;
#9892=FACE_OUTER_BOUND ( 'NONE', #44353, .T. ) ;
#9894=CARTESIAN_POINT ( 'NONE',  ( -101.5316874056614012, -25.03152356804190148, 7.138213056438796222 ) ) ;
#9895=CARTESIAN_POINT ( 'NONE',  ( -87.52287095715006160, -24.66019654487200086, 8.947790411086115725 ) ) ;
#9896=CARTESIAN_POINT ( 'NONE',  ( -0.4625342273119020797, 21.68341340789531912, -1.500000000000002220 ) ) ;
#9897=CARTESIAN_POINT ( 'NONE',  ( -78.62287095715005592, -29.50250786944525672, 11.44777988621623521 ) ) ;
#9898=CARTESIAN_POINT ( 'NONE',  ( -18.12599551585701008, -12.76988789260850332, 11.49999999999999645 ) ) ;
#9900=CARTESIAN_POINT ( 'NONE',  ( -98.89859089807453074, -25.27745440479792194, 5.967653818798817511 ) ) ;
#9902=ORIENTED_EDGE ( 'NONE', *, *, #39788, .T. ) ;
#9903=CARTESIAN_POINT ( 'NONE',  ( -20.89466310375201985, -8.809181082428260368, -1.500000000000002220 ) ) ;
#9904=EDGE_CURVE ( 'NONE', #34855, #41225, #35352, .T. ) ;
#9907=VERTEX_POINT ( 'NONE', #71202 ) ;
#9908=ORIENTED_EDGE ( 'NONE', *, *, #48589, .T. ) ;
#9911=AXIS2_PLACEMENT_3D ( 'NONE', #4818, #97657, #98143 ) ;
#9912=CARTESIAN_POINT ( 'NONE',  ( -17.93149374516376682, -9.230432107326475233, -1.500000000000002220 ) ) ;
#9914=ORIENTED_EDGE ( 'NONE', *, *, #12776, .T. ) ;
#9915=CARTESIAN_POINT ( 'NONE',  ( -42.62287095715006302, -23.96177878511307568, 10.65340807706330395 ) ) ;
#9916=CARTESIAN_POINT ( 'NONE',  ( 18.93296920960566965, -11.98514031388154599, -1.500000000000002220 ) ) ;
#9917=EDGE_CURVE ( 'NONE', #13466, #48086, #94028, .T. ) ;
#9922=CARTESIAN_POINT ( 'NONE',  ( -61.52287095715004739, -24.50321055353803956, 9.387540953477522265 ) ) ;
#9924=CARTESIAN_POINT ( 'NONE',  ( -130.5728709571500588, -24.26743686635981234, 0.04347934593174140189 ) ) ;
#9926=CARTESIAN_POINT ( 'NONE',  ( 2.036066721924049805, 19.47704226162102614, -1.500000000000002220 ) ) ;
#9927=CARTESIAN_POINT ( 'NONE',  ( -46.64649278270903920, -23.96119346886879953, -0.6495511937832144644 ) ) ;
#9929=VERTEX_POINT ( 'NONE', #88429 ) ;
#9930=CARTESIAN_POINT ( 'NONE',  ( 12.90647603486358364, 17.18646895862681134, -1.500000000000002220 ) ) ;
#9931=CARTESIAN_POINT ( 'NONE',  ( -128.6243649391845452, -23.48783264082479150, -1.443836473390056829 ) ) ;
#9933=CARTESIAN_POINT ( 'NONE',  ( -123.5228709571500474, -24.35013146730205236, 9.818937971375085283 ) ) ;
#9934=DIRECTION ( 'NONE',  ( 1.000000000000000000, 3.773278334444167608E-23, 8.201307833595939069E-29 ) ) ;
#9935=CARTESIAN_POINT ( 'NONE',  ( -17.45619364963476627, 14.87644265977633573, -1.500000000000002220 ) ) ;
#9936=ADVANCED_FACE ( 'NONE', ( #25012 ), #13278, .T. ) ;
#9937=EDGE_CURVE ( 'NONE', #54444, #31854, #53503, .T. ) ;
#9940=CARTESIAN_POINT ( 'NONE',  ( -42.52287095715006870, -23.73907113217662257, -1.053371485781402495 ) ) ;
#9941=CARTESIAN_POINT ( 'NONE',  ( -13.04681709000290013, -15.30929823114697541, 11.49999999999999645 ) ) ;
#9947=CARTESIAN_POINT ( 'NONE',  ( -17.59554656748941071, 9.132484154288260214, -1.500000000000002220 ) ) ;
#9948=EDGE_CURVE ( 'NONE', #33339, #45268, #12316, .T. ) ;
#9949=CARTESIAN_POINT ( 'NONE',  ( -4.706806674773570620, -21.25045708977441450, -1.500000000000002220 ) ) ;
#9950=DIRECTION ( 'NONE',  ( -1.000000000000000000, -3.773278334444166432E-23, -8.201307841325785021E-29 ) ) ;
#9951=CARTESIAN_POINT ( 'NONE',  ( -3.832734262880480358, 19.25313627021017382, -1.500000000000002220 ) ) ;
#9954=EDGE_CURVE ( 'NONE', #49044, #18516, #97034, .T. ) ;
#9955=CARTESIAN_POINT ( 'NONE',  ( -54.52287095715005449, -24.66019654487198665, 8.947790411086121054 ) ) ;
#9957=CARTESIAN_POINT ( 'NONE',  ( -103.5228709571500900, -23.72747288104470087, -1.053458166803225016 ) ) ;
#9959=CARTESIAN_POINT ( 'NONE',  ( -19.86366060283327784, 5.362777492974458049, 11.49999999999999645 ) ) ;
#9961=B_SPLINE_CURVE_WITH_KNOTS ( 'NONE', 3,
 ( #48980, #47976, #1802, #9399, #18515, #57600 ),
 .UNSPECIFIED., .F., .F.,
 ( 4, 2, 4 ),
 ( 6.384118694656723962E-06, 0.001386860460836396997, 0.002767336802978137555 ),
 .UNSPECIFIED. ) ;
#9963=CARTESIAN_POINT ( 'NONE',  ( 12.73759380600583846, -18.68238426224762350, 11.49999999999999645 ) ) ;
#9967=CARTESIAN_POINT ( 'NONE',  ( -97.58661751571909804, -24.51314013834315730, 0.6176544820404147318 ) ) ;
#9968=LINE ( 'NONE', #87599, #14270 ) ;
#9969=CARTESIAN_POINT ( 'NONE',  ( -26.72222193076970953, -24.93063575608347193, 7.978874889883705634 ) ) ;
#9970=CARTESIAN_POINT ( 'NONE',  ( -125.5895376238167245, -23.47596703998600631, 11.44779298504227683 ) ) ;
#9972=CARTESIAN_POINT ( 'NONE',  ( 21.75596283627254479, -7.788036635067100200, 11.49999999999999645 ) ) ;
#9973=CARTESIAN_POINT ( 'NONE',  ( -22.76716317511769461, -1.676022972194794791, 11.49999999999998934 ) ) ;
#9974=CARTESIAN_POINT ( 'NONE',  ( -110.6714443448221061, -25.19142773143022040, 3.340183518868431456 ) ) ;
#9976=CARTESIAN_POINT ( 'NONE',  ( -82.50599685478756840, -24.35071581493543036, 9.817618358456032368 ) ) ;
#9977=CARTESIAN_POINT ( 'NONE',  ( 21.68943130245101258, -6.005725296444199834, 11.49999999999999645 ) ) ;
#9978=ORIENTED_EDGE ( 'NONE', *, *, #77120, .T. ) ;
#9979=CARTESIAN_POINT ( 'NONE',  ( -43.48234448701215626, -24.65952944569304606, 1.056160979905694131 ) ) ;
#9981=CARTESIAN_POINT ( 'NONE',  ( -21.86317675896206225, -2.224439152981679602, 11.49999999999998934 ) ) ;
#9982=CARTESIAN_POINT ( 'NONE',  ( -127.4728709570019163, -25.40556189117671693, 4.803963375099988831 ) ) ;
#9986=CARTESIAN_POINT ( 'NONE',  ( -48.53562084801200882, -24.51419770103156637, 9.386484678747178734 ) ) ;
#9989=CARTESIAN_POINT ( 'NONE',  ( 20.06376955418885899, 4.186446014007643157, -1.500000000000002220 ) ) ;
#9990=VERTEX_POINT ( 'NONE', #66614 ) ;
#9991=ORIENTED_EDGE ( 'NONE', *, *, #52181, .F. ) ;
#9992=ORIENTED_EDGE ( 'NONE', *, *, #12897, .F. ) ;
#9993=ORIENTED_EDGE ( 'NONE', *, *, #79212, .F. ) ;
#9994=CARTESIAN_POINT ( 'NONE',  ( -84.62287095715005592, -23.48783264082479150, -1.443836473390065489 ) ) ;
#9995=CARTESIAN_POINT ( 'NONE',  ( 15.98122378838116120, 16.67787885001082770, -1.500000000000002220 ) ) ;
#9996=CARTESIAN_POINT ( 'NONE',  ( -63.92287095715007439, -23.47596703998600631, 11.44779298504227860 ) ) ;
#9997=CARTESIAN_POINT ( 'NONE',  ( 3.964343641299885146, 19.94596313931659992, -1.500000000000002220 ) ) ;
#9998=VERTEX_POINT ( 'NONE', #75673 ) ;
#10000=CARTESIAN_POINT ( 'NONE',  ( -51.34369400408914430, -25.18091725095096578, 3.196477947496687122 ) ) ;
#10002=CARTESIAN_POINT ( 'NONE',  ( -46.55620429048339304, -24.65952944569304606, 1.056160979905694797 ) ) ;
#10003=CARTESIAN_POINT ( 'NONE',  ( -63.52287095715007581, -24.50321055353804667, 9.387540953477527594 ) ) ;
#10004=CARTESIAN_POINT ( 'NONE',  ( -19.98823316618875268, 7.996883007359760320, 11.49999999999999645 ) ) ;
#10005=ORIENTED_EDGE ( 'NONE', *, *, #46233, .T. ) ;
#10006=CARTESIAN_POINT ( 'NONE',  ( -29.10059600771309007, -25.21531925493635740, 3.504324800834513809 ) ) ;
#10007=CARTESIAN_POINT ( 'NONE',  ( -49.26189073845563371, -25.26385756805315452, 4.538720795355990489 ) ) ;
#10009=ORIENTED_EDGE ( 'NONE', *, *, #43077, .F. ) ;
#10010=CARTESIAN_POINT ( 'NONE',  ( 6.562613027033147084, 19.67253995144353240, 11.49999999999998934 ) ) ;
#10011=EDGE_LOOP ( 'NONE', ( #82370, #55883, #93879, #19821 ) ) ;
#10012=CARTESIAN_POINT ( 'NONE',  ( -125.5215409636243606, -23.85016227208582151, -0.8807180028928047744 ) ) ;
#10015=CARTESIAN_POINT ( 'NONE',  ( -92.62287095715005592, -29.50250786944525672, 11.44777988621623344 ) ) ;
#10016=CARTESIAN_POINT ( 'NONE',  ( -51.89093686186974708, -25.27661087114319471, 5.843785486462916623 ) ) ;
#10018=ORIENTED_EDGE ( 'NONE', *, *, #93177, .F. ) ;
#10019=CARTESIAN_POINT ( 'NONE',  ( 2.021814659504407579E-13, -19.30000000000000426, -1.500000000000002220 ) ) ;
#10021=CARTESIAN_POINT ( 'NONE',  ( -30.64752034897746924, -23.47593901973090169, -1.443836447538997758 ) ) ;
#10022=CARTESIAN_POINT ( 'NONE',  ( 11.67614657018352453, 18.69773523334854914, 11.49999999999999645 ) ) ;
#10023=EDGE_LOOP ( 'NONE', ( #81029, #64190, #34250, #83507 ) ) ;
#10024=CARTESIAN_POINT ( 'NONE',  ( -49.02498481075217995, -25.18391117716921102, 6.789210593061082655 ) ) ;
#10025=CARTESIAN_POINT ( 'NONE',  ( -21.83012794225054165, -5.757306806698124113, -1.500000000000002220 ) ) ;
#10026=EDGE_CURVE ( 'NONE', #11110, #22234, #61941, .T. ) ;
#10027=EDGE_CURVE ( 'NONE', #38334, #98743, #12282, .T. ) ;
#10029=CARTESIAN_POINT ( 'NONE',  ( -80.96226385320382235, -25.13069340115295702, 2.947789388436138580 ) ) ;
#10031=ORIENTED_EDGE ( 'NONE', *, *, #84034, .T. ) ;
#10032=EDGE_CURVE ( 'NONE', #73391, #95103, #7461, .T. ) ;
#10033=CARTESIAN_POINT ( 'NONE',  ( -88.52287095715000476, -24.35013146730203815, 9.818937971375095941 ) ) ;
#10037=CARTESIAN_POINT ( 'NONE',  ( 9.152908845159860363, 19.05633030926415472, 11.49999999999998934 ) ) ;
#10038=CARTESIAN_POINT ( 'NONE',  ( -34.62287095715005592, -24.66019654487199020, 8.947790411086137041 ) ) ;
#10039=CARTESIAN_POINT ( 'NONE',  ( -51.93023907722363219, -25.03148449460395142, 6.217084953208106946 ) ) ;
#10041=CARTESIAN_POINT ( 'NONE',  ( -100.6228709571500559, -25.00158670708909625, 2.256160236439166411 ) ) ;
#10042=CARTESIAN_POINT ( 'NONE',  ( -18.24902840909259538, -12.68162010772806170, -1.500000000000002220 ) ) ;
#10044=EDGE_CURVE ( 'NONE', #53562, #52778, #73978, .T. ) ;
#10046=CARTESIAN_POINT ( 'NONE',  ( -112.5228709571500616, -23.48783264083431988, -1.443836473375253782 ) ) ;
#10047=CARTESIAN_POINT ( 'NONE',  ( -48.62287095715004881, -23.47593901973091235, -1.443836447539009749 ) ) ;
#10048=CARTESIAN_POINT ( 'NONE',  ( -15.52061920455031618, -11.66286593722069931, 11.49999999999999645 ) ) ;
#10049=CARTESIAN_POINT ( 'NONE',  ( -36.64213109380347078, -24.15620529776627379, 10.23563542870660825 ) ) ;
#10051=ADVANCED_FACE ( 'NONE', ( #76173 ), #45741, .T. ) ;
#10052=CARTESIAN_POINT ( 'NONE',  ( -15.31790942089943286, 12.02624123284522106, 11.49999999999998934 ) ) ;
#10053=CARTESIAN_POINT ( 'NONE',  ( -12.70309173801008562, -17.24390854791867511, 11.49999999999998934 ) ) ;
#10055=CARTESIAN_POINT ( 'NONE',  ( -60.59906223043246598, -24.15602025861359792, 10.28564288302606045 ) ) ;
#10056=VECTOR ( 'NONE', #86825, 1000.000000000000114 ) ;
#10057=CARTESIAN_POINT ( 'NONE',  ( -51.65198956701329536, -23.73766607897669445, -1.055555164236457788 ) ) ;
#10058=CARTESIAN_POINT ( 'NONE',  ( -91.52287095715006160, -23.47596703998600631, 11.44779298504228393 ) ) ;
#10059=B_SPLINE_CURVE_WITH_KNOTS ( 'NONE', 3,
 ( #14889, #46854, #92515, #6780, #37738, #31116 ),
 .UNSPECIFIED., .F., .F.,
 ( 4, 2, 4 ),
 ( 0.000000000000000000, 0.001380764517854760412, 0.002761529035709520824 ),
 .UNSPECIFIED. ) ;
#10060=CARTESIAN_POINT ( 'NONE',  ( 22.67573665902413182, 1.879276792517311501, -1.500000000000002220 ) ) ;
#10063=CARTESIAN_POINT ( 'NONE',  ( -102.5602245887073991, -23.48783264082478084, -1.443836473390064379 ) ) ;
#10065=CARTESIAN_POINT ( 'NONE',  ( 9.833179757865110560, 17.22857952739193266, 11.49999999999999645 ) ) ;
#10066=CARTESIAN_POINT ( 'NONE',  ( -123.5886720077133134, -24.66019654487200441, 8.947790411086106843 ) ) ;
#10070=CARTESIAN_POINT ( 'NONE',  ( -92.52287095715006160, -29.50250243563736774, 8.947779886222139822 ) ) ;
#10072=CARTESIAN_POINT ( 'NONE',  ( -71.52287095715003318, -23.95044443724991723, 10.65354141964649415 ) ) ;
#10073=CARTESIAN_POINT ( 'NONE',  ( 7.679218611123722837, 20.28660689097963399, -1.500000000000002220 ) ) ;
#10074=CARTESIAN_POINT ( 'NONE',  ( -56.55352364353050376, -23.96169478059713498, 10.65365249895718236 ) ) ;
#10075=CARTESIAN_POINT ( 'NONE',  ( -6.230579426152004885, -18.48807627814308674, -1.500000000000002220 ) ) ;
#10076=CARTESIAN_POINT ( 'NONE',  ( -55.51140977391407461, -23.85049219812686161, 10.88485053497527133 ) ) ;
#10079=VERTEX_POINT ( 'NONE', #14776 ) ;
#10081=CARTESIAN_POINT ( 'NONE',  ( 20.39576089869593289, -0.2533167397448486957, 11.49999999999999645 ) ) ;
#10082=CARTESIAN_POINT ( 'NONE',  ( -83.52287095715006160, -24.64965694238407323, 8.947790433994198267 ) ) ;
#10088=CARTESIAN_POINT ( 'NONE',  ( -114.5228709571500758, -23.47593901973090524, -1.443836447538996204 ) ) ;
#10089=CARTESIAN_POINT ( 'NONE',  ( -50.52287095715006160, -23.48783264082477018, -1.443836473390095021 ) ) ;
#10092=ORIENTED_EDGE ( 'NONE', *, *, #57819, .F. ) ;
#10093=CARTESIAN_POINT ( 'NONE',  ( -66.50057777483888799, -24.35071581493543036, 9.817618358456028815 ) ) ;
#10094=CARTESIAN_POINT ( 'NONE',  ( -22.77861398648627400, -3.026084143414268013, 11.49999999999999645 ) ) ;
#10095=CARTESIAN_POINT ( 'NONE',  ( 22.50852769316577096, -3.342225187595919689, -1.500000000000002220 ) ) ;
#10097=B_SPLINE_SURFACE_WITH_KNOTS ( 'NONE', 3, 3, ( 
 ( #91363, #90868, #6128, #52317 ),
 ( #16121, #47091, #78007, #21339 ),
 ( #83251, #37081, #21839, #8519 ),
 ( #70421, #98970, #62829, #13732 ),
 ( #63328, #60442, #93743, #86139 ),
 ( #47593, #64843, #95753, #19620 ),
 ( #41988, #11510, #27250, #72431 ) ),
 .UNSPECIFIED., .F., .F., .F.,
 ( 4, 3, 4 ),
 ( 4, 4 ),
 ( 0.7945040050992245861, 0.8970133687736505657, 0.9995227324480766562 ),
 ( 0.8897200874468342846, 0.8911435658352574452 ),
 .UNSPECIFIED. ) ;
#10099=CARTESIAN_POINT ( 'NONE',  ( -123.5895376238167103, -24.66019654487199730, 8.947790411086122830 ) ) ;
#10100=B_SPLINE_CURVE_WITH_KNOTS ( 'NONE', 3,
 ( #75668, #84790, #62, #13769 ),
 .UNSPECIFIED., .F., .F.,
 ( 4, 4 ),
 ( 0.000000000000000000, 1.000000000000000000 ),
 .UNSPECIFIED. ) ;
#10102=CARTESIAN_POINT ( 'NONE',  ( -6.542779104410481494, 20.88585256366161502, 11.49999999999998934 ) ) ;
#10103=FACE_OUTER_BOUND ( 'NONE', #50721, .T. ) ;
#10105=CARTESIAN_POINT ( 'NONE',  ( -48.97733596696294711, -25.30014187938330039, 5.627950841079814026 ) ) ;
#10106=CARTESIAN_POINT ( 'NONE',  ( -122.5535501483336702, -24.65952944569305316, 1.056160979905708786 ) ) ;
#10107=FACE_OUTER_BOUND ( 'NONE', #62084, .T. ) ;
#10108=ORIENTED_EDGE ( 'NONE', *, *, #75428, .T. ) ;
#10109=CARTESIAN_POINT ( 'NONE',  ( -20.42006937447004233, 0.3101567295262241952, 11.49999999999998934 ) ) ;
#10110=ORIENTED_EDGE ( 'NONE', *, *, #39112, .T. ) ;
#10112=CARTESIAN_POINT ( 'NONE',  ( -23.02147672596084149, 0.6323230698326208765, 11.49999999999998934 ) ) ;
#10116=LINE ( 'NONE', #61537, #31964 ) ;
#10117=CARTESIAN_POINT ( 'NONE',  ( -59.27315685164825965, -25.27306215940455658, 3.719512753259344606 ) ) ;
#10119=CARTESIAN_POINT ( 'NONE',  ( 19.49461108348020133, 8.573440864381753457, 11.49999999999999645 ) ) ;
#10120=VERTEX_POINT ( 'NONE', #85294 ) ;
#10122=ORIENTED_EDGE ( 'NONE', *, *, #37403, .T. ) ;
#10123=CARTESIAN_POINT ( 'NONE',  ( 12.24756355222007898, 18.56953561607567238, -1.500000000000002220 ) ) ;
#10124=CARTESIAN_POINT ( 'NONE',  ( 20.62939718826500979, -0.8834638802319035866, -1.500000000000002220 ) ) ;
#10127=CARTESIAN_POINT ( 'NONE',  ( -95.55036893831936595, -24.40133493613050319, 9.663955038902802386 ) ) ;
#10128=ORIENTED_EDGE ( 'NONE', *, *, #76248, .F. ) ;
#10131=VERTEX_POINT ( 'NONE', #91402 ) ;
#10132=CARTESIAN_POINT ( 'NONE',  ( -129.5228709571500758, -24.65952944569305316, 1.056160979905707675 ) ) ;
#10135=CARTESIAN_POINT ( 'NONE',  ( 17.12911088700535700, -11.98135219954639830, -1.500000000000002220 ) ) ;
#10136=CARTESIAN_POINT ( 'NONE',  ( -20.59625928752216240, -7.366027188055905839, 11.49999999999999645 ) ) ;
#10137=B_SPLINE_CURVE_WITH_KNOTS ( 'NONE', 3,
 ( #55372, #49768, #48259, #86306, #80698, #56384 ),
 .UNSPECIFIED., .F., .F.,
 ( 4, 2, 4 ),
 ( 0.000000000000000000, 0.001380764517854761279, 0.002761529035709522559 ),
 .UNSPECIFIED. ) ;
#10139=CARTESIAN_POINT ( 'NONE',  ( -26.35118574718723750, -24.89279778413545330, 6.568084036181874197 ) ) ;
#10141=CARTESIAN_POINT ( 'NONE',  ( 5.133194422563156500, 21.89913303424002677, -1.500000000000002220 ) ) ;
#10142=EDGE_CURVE ( 'NONE', #30369, #14722, #98221, .T. ) ;
#10143=CARTESIAN_POINT ( 'NONE',  ( 4.013313563623547964, -20.52093592976233438, 11.49999999999998934 ) ) ;
#10144=CARTESIAN_POINT ( 'NONE',  ( -38.57583223673756123, -24.65952944569304606, 1.056160979905694131 ) ) ;
#10150=EDGE_LOOP ( 'NONE', ( #25686, #44797, #91480, #5191 ) ) ;
#10151=ORIENTED_EDGE ( 'NONE', *, *, #84216, .T. ) ;
#10152=CARTESIAN_POINT ( 'NONE',  ( -52.55339754476869274, -23.96119346886881019, -0.6495511937831939253 ) ) ;
#10154=CARTESIAN_POINT ( 'NONE',  ( -20.93543047832761417, 4.563121699532205255, -1.500000000000002220 ) ) ;
#10156=ADVANCED_FACE ( 'NONE', ( #47246 ), #60320, .T. ) ;
#10157=CARTESIAN_POINT ( 'NONE',  ( 1.438201247614206757, 22.34484416265529916, 11.49999999999999645 ) ) ;
#10158=VERTEX_POINT ( 'NONE', #23379 ) ;
#10160=CARTESIAN_POINT ( 'NONE',  ( -10.38599875782317206, -18.32754119035049101, 11.49999999999998934 ) ) ;
#10161=CARTESIAN_POINT ( 'NONE',  ( -30.61200487207880983, -24.39002261744410660, 9.702671485061733492 ) ) ;
#10162=CARTESIAN_POINT ( 'NONE',  ( -19.52388446859773552, -3.948942086532154061, -1.500000000000002220 ) ) ;
#10163=CARTESIAN_POINT ( 'NONE',  ( -50.52962757068328159, -24.83644354573578639, 8.397322867130096569 ) ) ;
#10164=CARTESIAN_POINT ( 'NONE',  ( -80.88924702628075636, -25.29534364326325857, 4.592921242107371960 ) ) ;
#10165=CARTESIAN_POINT ( 'NONE',  ( -22.03165466229905789, 1.424673820674137614, -1.500000000000002220 ) ) ;
#10167=VERTEX_POINT ( 'NONE', #562 ) ;
#10168=CARTESIAN_POINT ( 'NONE',  ( -65.48373211964047869, -25.00182538069146432, 7.747789668545041586 ) ) ;
#10170=CARTESIAN_POINT ( 'NONE',  ( -60.48284454307438551, -24.92564183028978775, 1.928384488918253092 ) ) ;
#10171=CARTESIAN_POINT ( 'NONE',  ( -62.55372391215821892, -23.96169478059712787, 10.65365249895718414 ) ) ;
#10175=CARTESIAN_POINT ( 'NONE',  ( -9.236746577462426444, 19.23066362772381055, -1.500000000000002220 ) ) ;
#10176=CARTESIAN_POINT ( 'NONE',  ( -97.62287095715005592, -24.66019654487200086, 8.947790411086124607 ) ) ;
#10177=CARTESIAN_POINT ( 'NONE',  ( -51.29687923781919068, -25.27367468601215350, 3.993462154588707680 ) ) ;
#10179=CARTESIAN_POINT ( 'NONE',  ( -81.04674198455134615, -25.14820543576475487, 6.953655299421349412 ) ) ;
#10180=CARTESIAN_POINT ( 'NONE',  ( 21.16815136333514502, -7.790938087775149512, -1.500000000000002220 ) ) ;
#10181=VECTOR ( 'NONE', #60239, 1000.000000000000114 ) ;
#10182=B_SPLINE_SURFACE_WITH_KNOTS ( 'NONE', 3, 3, ( 
 ( #96230, #57185, #2892, #66292 ),
 ( #50549, #12970, #74379, #80494 ),
 ( #64809, #72398, #66796, #18587 ),
 ( #88120, #81502, #19088, #73885 ),
 ( #26213, #42455, #49563, #4877 ),
 ( #97223, #20585, #27714, #72898 ),
 ( #26712, #97715, #50059, #80999 ) ),
 .UNSPECIFIED., .F., .F., .F.,
 ( 4, 3, 4 ),
 ( 4, 4 ),
 ( 0.0004766839783823150411, 0.1029713700210899557, 0.2054660560637975864 ),
 ( 0.1895422135489633897, 0.1906423925340593462 ),
 .UNSPECIFIED. ) ;
#10183=CARTESIAN_POINT ( 'NONE',  ( -51.52287095715008292, -24.35013146730202749, 9.818937971375104823 ) ) ;
#10184=VERTEX_POINT ( 'NONE', #31510 ) ;
#10185=DIRECTION ( 'NONE',  ( 1.000000000000000000, 3.773278334444166432E-23, 8.201307841325785021E-29 ) ) ;
#10186=CARTESIAN_POINT ( 'NONE',  ( -31.52200024016721969, -23.48786465467240347, 11.44779295918255535 ) ) ;
#10187=CARTESIAN_POINT ( 'NONE',  ( 9.421224358276909072, -17.24829524558457194, 11.49999999999999645 ) ) ;
#10190=ORIENTED_EDGE ( 'NONE', *, *, #91939, .T. ) ;
#10191=CARTESIAN_POINT ( 'NONE',  ( -29.62287095715004881, -29.50250473134420659, 10.00399446418115268 ) ) ;
#10192=CARTESIAN_POINT ( 'NONE',  ( -124.4728709594060376, -25.40676174399605713, 8.000950338062997602 ) ) ;
#10195=PLANE ( 'NONE',  #68033 ) ;
#10196=CARTESIAN_POINT ( 'NONE',  ( -32.82970096230013013, -25.05419505390707968, 2.466848186059392045 ) ) ;
#10197=CARTESIAN_POINT ( 'NONE',  ( -68.55620429048339304, -24.64965694238574656, 8.947790433994198267 ) ) ;
#10198=EDGE_CURVE ( 'NONE', #26695, #31094, #76466, .T. ) ;
#10199=CARTESIAN_POINT ( 'NONE',  ( -13.31955177964949755, -14.60123061082138385, 11.49999999999998934 ) ) ;
#10200=ORIENTED_EDGE ( 'NONE', *, *, #86589, .T. ) ;
#10202=CARTESIAN_POINT ( 'NONE',  ( -19.95319933381289701, -3.276446921841525306, 11.49999999999999645 ) ) ;
#10207=CARTESIAN_POINT ( 'NONE',  ( -81.10370361591597543, -25.30541368948374981, 5.079816334721119375 ) ) ;
#10209=CARTESIAN_POINT ( 'NONE',  ( -115.5228709571500616, -23.47596703998600631, 11.44779298504227860 ) ) ;
#10211=CARTESIAN_POINT ( 'NONE',  ( -71.62287095715002749, -24.50216790748206108, 0.6166512839542562796 ) ) ;
#10212=CARTESIAN_POINT ( 'NONE',  ( -16.84340083857899018, -10.81494551495373457, -1.500000000000002220 ) ) ;
#10213=CARTESIAN_POINT ( 'NONE',  ( -99.12380231474227799, -25.27533115719222678, 4.001575131757423520 ) ) ;
#10214=ORIENTED_EDGE ( 'NONE', *, *, #99789, .F. ) ;
#10215=VECTOR ( 'NONE', #93293, 1000.000000000000114 ) ;
#10216=B_SPLINE_CURVE_WITH_KNOTS ( 'NONE', 3,
 ( #34506, #19755, #50731, #57362, #3066, #81676, #64982, #41629, #94014, #88294 ),
 .UNSPECIFIED., .F., .F.,
 ( 4, 2, 2, 2, 4 ),
 ( 2.602085213965210642E-18, 0.0002062928591221676493, 0.0004125857182443326966, 0.0008251714364886473954, 0.001650342872977302380 ),
 .UNSPECIFIED. ) ;
#10219=CARTESIAN_POINT ( 'NONE',  ( -33.62287095715005592, -23.48783264082477373, -1.443836473390074371 ) ) ;
#10220=CARTESIAN_POINT ( 'NONE',  ( -63.62287095715004881, -24.64965695001468404, 8.947790433994185832 ) ) ;
#10221=CARTESIAN_POINT ( 'NONE',  ( -38.55620429048340014, -23.48783264082477373, -1.443836473390072817 ) ) ;
#10222=CARTESIAN_POINT ( 'NONE',  ( -103.5228709571501042, -23.73907113216989373, -1.053371485793248574 ) ) ;
#10225=CARTESIAN_POINT ( 'NONE',  ( -49.65333006503131941, -25.22444173014155666, 3.599674781239922350 ) ) ;
#10227=CARTESIAN_POINT ( 'NONE',  ( 20.05691770114479766, 3.104179615465487707, 11.49999999999998934 ) ) ;
#10228=VERTEX_POINT ( 'NONE', #25905 ) ;
#10230=CARTESIAN_POINT ( 'NONE',  ( -122.5228709571500332, -23.48783264082477018, -1.443836473390084807 ) ) ;
#10231=CARTESIAN_POINT ( 'NONE',  ( -59.55362377784436489, -23.96169478059712787, 10.65365249895718769 ) ) ;
#10232=CARTESIAN_POINT ( 'NONE',  ( -83.58953762381673869, -23.48786465467241769, 11.44779295918254469 ) ) ;
#10233=CARTESIAN_POINT ( 'NONE',  ( -65.62287095715008434, -23.84081130438201868, 10.88220057463249191 ) ) ;
#10234=CARTESIAN_POINT ( 'NONE',  ( -19.86647519178106691, -7.318714840676754818, 11.49999999999999645 ) ) ;
#10235=CARTESIAN_POINT ( 'NONE',  ( -18.17467834739497690, 12.62983929299386965, 11.49999999999998934 ) ) ;
#10236=CARTESIAN_POINT ( 'NONE',  ( -4.563637348303267949, -20.04915943051449645, 11.49999999999998934 ) ) ;
#10237=VERTEX_POINT ( 'NONE', #17798 ) ;
#10238=CARTESIAN_POINT ( 'NONE',  ( -116.5228709571500616, -24.64965694238575011, 8.947790433994191162 ) ) ;
#10239=ORIENTED_EDGE ( 'NONE', *, *, #93816, .F. ) ;
#10240=CARTESIAN_POINT ( 'NONE',  ( -54.52206328644955846, -23.48783264082476663, -1.443836473390098130 ) ) ;
#10241=CARTESIAN_POINT ( 'NONE',  ( -110.6228709571500701, -25.00182538069145011, 7.747789668545099317 ) ) ;
#10244=ORIENTED_EDGE ( 'NONE', *, *, #48241, .F. ) ;
#10247=CARTESIAN_POINT ( 'NONE',  ( -111.4287875950415554, -25.20169993477061254, 3.340150141510382031 ) ) ;
#10248=CARTESIAN_POINT ( 'NONE',  ( -127.6228709571500275, -24.51387760970724372, 9.387446482453405849 ) ) ;
#10250=CARTESIAN_POINT ( 'NONE',  ( -19.01758589260300525, -8.224767016273846210, -1.500000000000002220 ) ) ;
#10251=CARTESIAN_POINT ( 'NONE',  ( 8.597998336517790108, -19.88058937513707392, 11.49999999999999645 ) ) ;
#10252=VERTEX_POINT ( 'NONE', #41144 ) ;
#10254=ADVANCED_FACE ( 'NONE', ( #1072 ), #3087, .T. ) ;
#10255=CARTESIAN_POINT ( 'NONE',  ( -60.52287095715007581, -24.92604778743751481, 8.074972756821495068 ) ) ;
#10257=CARTESIAN_POINT ( 'NONE',  ( 21.16571772479873204, -7.350578744355993344, 11.49999999999998934 ) ) ;
#10260=CARTESIAN_POINT ( 'NONE',  ( -102.5228709571500758, -24.51387760970725438, 9.387446482453409402 ) ) ;
#10265=EDGE_CURVE ( 'NONE', #83981, #84492, #96970, .T. ) ;
#10268=ORIENTED_EDGE ( 'NONE', *, *, #74509, .F. ) ;
#10269=CARTESIAN_POINT ( 'NONE',  ( -71.22287095715005023, -23.47596703998600276, 11.44779298504227860 ) ) ;
#10270=ORIENTED_EDGE ( 'NONE', *, *, #14986, .T. ) ;
#10271=CARTESIAN_POINT ( 'NONE',  ( -51.52764846858840997, -29.50249643624320584, 6.187563540074810575 ) ) ;
#10272=CARTESIAN_POINT ( 'NONE',  ( -21.08002519818654363, -2.465602145356518893, -1.500000000000002220 ) ) ;
#10273=ORIENTED_EDGE ( 'NONE', *, *, #45664, .T. ) ;
#10274=DIRECTION ( 'NONE',  ( 0.000000000000000000, 0.9999999999976377785, 2.173523156925979975E-06 ) ) ;
#10275=CARTESIAN_POINT ( 'NONE',  ( -13.95179422449595208, 16.79422078803934326, 11.49999999999998934 ) ) ;
#10276=CARTESIAN_POINT ( 'NONE',  ( -103.5113892122844277, -24.51419770103155926, 9.386484678747176957 ) ) ;
#10277=PLANE ( 'NONE',  #77711 ) ;
#10279=CARTESIAN_POINT ( 'NONE',  ( 15.24057855588860377, 15.72025634131890470, -1.500000000000002220 ) ) ;
#10282=EDGE_CURVE ( 'NONE', #9142, #59928, #70373, .T. ) ;
#10283=DIRECTION ( 'NONE',  ( -3.773278334453080206E-23, 0.9999999999976377785, 2.173523156925979975E-06 ) ) ;
#10284=CARTESIAN_POINT ( 'NONE',  ( -48.89385731722059347, -25.26337357799507544, 6.392748942997004136 ) ) ;
#10287=AXIS2_PLACEMENT_3D ( 'NONE', #41245, #175, #54971 ) ;
#10288=ORIENTED_EDGE ( 'NONE', *, *, #62222, .F. ) ;
#10289=CARTESIAN_POINT ( 'NONE',  ( -58.58953762381673158, -24.64965694238407323, 8.947790433994656567 ) ) ;
#10290=CARTESIAN_POINT ( 'NONE',  ( -31.24388727629347429, -25.01990435277411606, 2.279866971661216546 ) ) ;
#10291=CARTESIAN_POINT ( 'NONE',  ( -10.85727797829764185, 18.24708236899833835, 11.49999999999998934 ) ) ;
#10292=CARTESIAN_POINT ( 'NONE',  ( -125.5895376238167245, -25.00182538069145721, 7.747789668545099317 ) ) ;
#10293=DIRECTION ( 'NONE',  ( 0.000000000000000000, 0.9999999999976377785, 2.173523156925979975E-06 ) ) ;
#10295=CARTESIAN_POINT ( 'NONE',  ( -118.5228709571500758, -29.50247984919015209, -1.443849546365046699 ) ) ;
#10297=CARTESIAN_POINT ( 'NONE',  ( -19.30698013599780083, -2.078282243779251637, -1.500000000000002220 ) ) ;
#10298=CARTESIAN_POINT ( 'NONE',  ( -117.5885002923016884, -24.51419770103158768, 9.386484678747164523 ) ) ;
#10300=CARTESIAN_POINT ( 'NONE',  ( 13.27039818535887505, -14.28956163997708906, 11.49999999999999645 ) ) ;
#10302=AXIS2_PLACEMENT_3D ( 'NONE', #22747, #30878, #47118 ) ;
#10303=DIRECTION ( 'NONE',  ( -3.773278334453079618E-23, 0.9999999999976377785, 2.173523156925979975E-06 ) ) ;
#10307=CARTESIAN_POINT ( 'NONE',  ( -89.58586318894654710, -24.51314013834317151, 0.6176544820404251679 ) ) ;
#10309=EDGE_CURVE ( 'NONE', #27242, #75398, #22012, .T. ) ;
#10310=CARTESIAN_POINT ( 'NONE',  ( -117.6228709571500559, -29.50250786944525672, 11.44777988621622811 ) ) ;
#10311=CARTESIAN_POINT ( 'NONE',  ( -10.66912846187372210, -16.51573522771486324, 11.49999999999998934 ) ) ;
#10312=ORIENTED_EDGE ( 'NONE', *, *, #89855, .F. ) ;
#10314=CARTESIAN_POINT ( 'NONE',  ( 17.26854690438276307, -15.35948741044508559, -1.500000000000002220 ) ) ;
#10316=EDGE_CURVE ( 'NONE', #45280, #8769, #9807, .T. ) ;
#10318=DIRECTION ( 'NONE',  ( 1.000000000000000000, 3.773278334444167608E-23, 8.201307833595939069E-29 ) ) ;
#10319=CARTESIAN_POINT ( 'NONE',  ( -79.52287095715006160, -24.66019654487199375, 8.947790411086122830 ) ) ;
#10320=CARTESIAN_POINT ( 'NONE',  ( -97.54989192072140725, -24.35071581493543746, 9.817618358456025263 ) ) ;
#10321=CARTESIAN_POINT ( 'NONE',  ( -80.90972592788718032, -25.29489613318244423, 6.057562805997258160 ) ) ;
#10322=CARTESIAN_POINT ( 'NONE',  ( -43.62287095715003460, -23.73934037231756733, 11.05740245334329153 ) ) ;
#10323=CARTESIAN_POINT ( 'NONE',  ( -68.62287095715005592, -29.50250243563736774, 8.947779886222143375 ) ) ;
#10324=CARTESIAN_POINT ( 'NONE',  ( -50.62287095715007013, -24.62226745350439572, 0.9660975649728152925 ) ) ;
#10325=CARTESIAN_POINT ( 'NONE',  ( -1.646307629438301667, 19.86461321233117872, -1.500000000000002220 ) ) ;
#10328=CARTESIAN_POINT ( 'NONE',  ( -75.53594935777978492, -24.92592662359561118, 8.075495903018000021 ) ) ;
#10329=CARTESIAN_POINT ( 'NONE',  ( -12.84220538718065185, 15.17226672225704398, -1.500000000000002220 ) ) ;
#10330=ORIENTED_EDGE ( 'NONE', *, *, #88660, .F. ) ;
#10331=CARTESIAN_POINT ( 'NONE',  ( -90.70643032827079821, -25.32958289424478338, 5.296252972553156191 ) ) ;
#10333=CARTESIAN_POINT ( 'NONE',  ( -125.5228709571501184, -23.84047902841604127, -0.8780736468305687659 ) ) ;
#10336=CARTESIAN_POINT ( 'NONE',  ( -11.07951500695464553, -17.62175104703424466, 11.49999999999999645 ) ) ;
#10339=CARTESIAN_POINT ( 'NONE',  ( -50.40445135320380388, -25.18492896333868103, 3.293943116708552221 ) ) ;
#10340=CARTESIAN_POINT ( 'NONE',  ( 21.15473741701296362, -8.388382055385795510, 11.49999999999999645 ) ) ;
#10341=ORIENTED_EDGE ( 'NONE', *, *, #68339, .F. ) ;
#10345=CARTESIAN_POINT ( 'NONE',  ( 15.73562052650688514, -12.66937975264744587, 11.49999999999998934 ) ) ;
#10347=CARTESIAN_POINT ( 'NONE',  ( -41.03061461742554883, -25.30559429607382782, 4.924307031744522334 ) ) ;
#10348=CARTESIAN_POINT ( 'NONE',  ( -100.6228709571500559, -25.00158670708909625, 2.256160236439166411 ) ) ;
#10349=VERTEX_POINT ( 'NONE', #26410 ) ;
#10352=CARTESIAN_POINT ( 'NONE',  ( -6.099057486122481997, -19.05896565686126110, -1.500000000000002220 ) ) ;
#10353=CARTESIAN_POINT ( 'NONE',  ( 15.12549221760053086, 14.48511125727034177, 11.49999999999999645 ) ) ;
#10356=CARTESIAN_POINT ( 'NONE',  ( 13.08019894233326319, 17.74467248152726384, 11.49999999999998934 ) ) ;
#10357=CARTESIAN_POINT ( 'NONE',  ( -42.62287095715004881, -24.64898659630367561, 1.056161002820819261 ) ) ;
#10359=CARTESIAN_POINT ( 'NONE',  ( -82.52287095715006160, -29.50250786944525672, 11.44777988621623521 ) ) ;
#10360=CARTESIAN_POINT ( 'NONE',  ( -49.54012794836013001, -25.18440211203497725, 3.796733314902499767 ) ) ;
#10361=CARTESIAN_POINT ( 'NONE',  ( -74.62287095715005592, -24.64965695001467694, 8.947790433994184056 ) ) ;
#10362=ORIENTED_EDGE ( 'NONE', *, *, #83422, .F. ) ;
#10363=FACE_OUTER_BOUND ( 'NONE', #49297, .T. ) ;
#10364=ORIENTED_EDGE ( 'NONE', *, *, #52752, .F. ) ;
#10365=ORIENTED_EDGE ( 'NONE', *, *, #38650, .T. ) ;
#10366=ADVANCED_FACE ( 'NONE', ( #32517 ), #71591, .T. ) ;
#10370=CARTESIAN_POINT ( 'NONE',  ( 18.67943556539783856, 8.552475402716291697, -1.500000000000002220 ) ) ;
#10371=ORIENTED_EDGE ( 'NONE', *, *, #34119, .F. ) ;
#10372=LINE ( 'NONE', #95613, #18648 ) ;
#10373=CARTESIAN_POINT ( 'NONE',  ( -38.52287095715006870, -24.65952944569303895, 1.056160979905691910 ) ) ;
#10374=CARTESIAN_POINT ( 'NONE',  ( -41.52287095715007581, -24.50321055353804667, 9.387540953477524042 ) ) ;
#10375=CARTESIAN_POINT ( 'NONE',  ( 7.190675130926929448, -21.12231643677837312, 11.49999999999998934 ) ) ;
#10377=LINE ( 'NONE', #94107, #44830 ) ;
#10383=CARTESIAN_POINT ( 'NONE',  ( -14.93763623016880082, -14.57113377498261997, 11.49999999999998934 ) ) ;
#10388=ORIENTED_EDGE ( 'NONE', *, *, #10614, .F. ) ;
#10389=CARTESIAN_POINT ( 'NONE',  ( -69.62994293422308090, -25.25935311477814693, 7.382559191806408627 ) ) ;
#10390=CARTESIAN_POINT ( 'NONE',  ( -20.88184962559319402, -2.832954952542597660, -1.500000000000002220 ) ) ;
#10391=ORIENTED_EDGE ( 'NONE', *, *, #83780, .T. ) ;
#10395=CARTESIAN_POINT ( 'NONE',  ( -86.59502610026325442, -23.96169478059713498, 10.65365249895717881 ) ) ;
#10396=CARTESIAN_POINT ( 'NONE',  ( -59.59291227190924189, -24.15543982623906416, -0.2315651400026668416 ) ) ;
#10397=CARTESIAN_POINT ( 'NONE',  ( -19.97641003480726241, 8.421946895145676848, -1.500000000000002220 ) ) ;
#10399=CARTESIAN_POINT ( 'NONE',  ( 18.07686251855496096, -12.98574554580779861, 11.49999999999999645 ) ) ;
#10400=ORIENTED_EDGE ( 'NONE', *, *, #47148, .T. ) ;
#10404=CARTESIAN_POINT ( 'NONE',  ( -70.35895856474229504, -25.30161620421289470, 5.313173632321669615 ) ) ;
#10408=ORIENTED_EDGE ( 'NONE', *, *, #42828, .T. ) ;
#10409=VECTOR ( 'NONE', #52928, 1000.000000000000114 ) ;
#10412=CARTESIAN_POINT ( 'NONE',  ( 19.84801528777503776, 3.447069022702595742, -1.500000000000002220 ) ) ;
#10413=LINE ( 'NONE', #96160, #53861 ) ;
#10414=ORIENTED_EDGE ( 'NONE', *, *, #34564, .F. ) ;
#10415=CARTESIAN_POINT ( 'NONE',  ( -130.5728709571500588, -25.05579301371511747, 7.915991903154699472 ) ) ;
#10416=CARTESIAN_POINT ( 'NONE',  ( -21.16225983376422448, 7.283793490815352989, -1.500000000000002220 ) ) ;
#10417=EDGE_LOOP ( 'NONE', ( #7144, #34230, #51084, #4510 ) ) ;
#10418=ORIENTED_EDGE ( 'NONE', *, *, #2962, .F. ) ;
#10420=CARTESIAN_POINT ( 'NONE',  ( -101.6367508631515477, -23.48786465467240703, 11.44779295918254114 ) ) ;
#10421=CARTESIAN_POINT ( 'NONE',  ( -67.62287095715005592, -24.64965695001468404, 8.947790433994184056 ) ) ;
#10422=CARTESIAN_POINT ( 'NONE',  ( -56.52287095715006870, -29.50250243563736774, 8.947779886222145151 ) ) ;
#10423=CARTESIAN_POINT ( 'NONE',  ( -63.91869748439341237, -24.82959736273286921, 8.370978854367633559 ) ) ;
#10425=CARTESIAN_POINT ( 'NONE',  ( -6.824658503225996320, 18.35159230250476270, -1.500000000000002220 ) ) ;
#10427=ORIENTED_EDGE ( 'NONE', *, *, #25961, .T. ) ;
#10428=CARTESIAN_POINT ( 'NONE',  ( -15.45034113870702441, -14.97902827799142500, -1.500000000000002220 ) ) ;
#10430=CARTESIAN_POINT ( 'NONE',  ( -80.43221577628075636, -25.31572646011074212, 4.967019755498037981 ) ) ;
#10433=CARTESIAN_POINT ( 'NONE',  ( -22.24355531667433539, 5.575215412481045796, -1.500000000000002220 ) ) ;
#10436=CARTESIAN_POINT ( 'NONE',  ( -89.81226385320383088, -25.27880950044345454, 5.947789066509452383 ) ) ;
#10437=CARTESIAN_POINT ( 'NONE',  ( -53.63293900283483140, -24.34968618360933590, 0.1864209137778786440 ) ) ;
#10438=CARTESIAN_POINT ( 'NONE',  ( -19.68739882612603864, 4.164723872966736629, 11.49999999999999645 ) ) ;
#10439=CARTESIAN_POINT ( 'NONE',  ( -40.62287095715004170, -25.00182538069145011, 7.747789668545099317 ) ) ;
#10441=DIRECTION ( 'NONE',  ( -3.773278334453079030E-23, 0.9999999999976377785, 2.173523156925979128E-06 ) ) ;
#10442=DIRECTION ( 'NONE',  ( 0.000000000000000000, 0.9999999999976377785, 2.173523156925979975E-06 ) ) ;
#10445=CARTESIAN_POINT ( 'NONE',  ( -15.99800673754971037, 11.70972097625665675, -1.500000000000002220 ) ) ;
#10447=CARTESIAN_POINT ( 'NONE',  ( -2.340448316220725467, 19.49152957720520618, -1.500000000000002220 ) ) ;
#10448=CARTESIAN_POINT ( 'NONE',  ( -42.56928426289123735, -23.48783264082477373, -1.443836473390076147 ) ) ;
#10449=CARTESIAN_POINT ( 'NONE',  ( -58.52287095715006160, -23.48786465467241058, 11.44779295918254824 ) ) ;
#10451=CARTESIAN_POINT ( 'NONE',  ( -60.52287095715007581, -24.82576562948885623, 8.398263436605553522 ) ) ;
#10452=CARTESIAN_POINT ( 'NONE',  ( -39.15118670841629012, -25.30439178025131142, 4.799404196304809744 ) ) ;
#10453=CARTESIAN_POINT ( 'NONE',  ( -18.12278953325389708, -9.833843834435361586, 11.49999999999999645 ) ) ;
#10454=FACE_OUTER_BOUND ( 'NONE', #72545, .T. ) ;
#10455=B_SPLINE_CURVE_WITH_KNOTS ( 'NONE', 3,
 ( #7476, #44052, #74984, #29819 ),
 .UNSPECIFIED., .F., .F.,
 ( 4, 4 ),
 ( 0.000000000000000000, 9.999999999998897304E-05 ),
 .UNSPECIFIED. ) ;
#10456=AXIS2_PLACEMENT_3D ( 'NONE', #77806, #39263, #39760 ) ;
#10457=EDGE_CURVE ( 'NONE', #59016, #11739, #14659, .T. ) ;
#10459=CARTESIAN_POINT ( 'NONE',  ( -4.885077187424587741, 22.05487924249641551, 11.49999999999999645 ) ) ;
#10461=CARTESIAN_POINT ( 'NONE',  ( -53.55620429048339304, -24.65952944569304606, 1.056160979905692576 ) ) ;
#10462=CARTESIAN_POINT ( 'NONE',  ( -51.07385796617099061, -25.30408280926228670, 4.469399184940273884 ) ) ;
#10463=CARTESIAN_POINT ( 'NONE',  ( -128.6228709571500417, -24.66019654487200441, 8.947790411086121054 ) ) ;
#10464=CARTESIAN_POINT ( 'NONE',  ( -110.5228709571500474, -24.52232992886363050, 0.6492154411906037037 ) ) ;
#10465=AXIS2_PLACEMENT_3D ( 'NONE', #64828, #41459, #82012 ) ;
#10467=EDGE_CURVE ( 'NONE', #34684, #15382, #65497, .T. ) ;
#10468=EDGE_CURVE ( 'NONE', #49598, #41774, #69102, .T. ) ;
#10469=ORIENTED_EDGE ( 'NONE', *, *, #68209, .F. ) ;
#10471=CARTESIAN_POINT ( 'NONE',  ( -22.55118551311790753, 3.560990644294375063, 11.49999999999998934 ) ) ;
#10472=CARTESIAN_POINT ( 'NONE',  ( -111.3164332061762991, -25.26394802776237114, 3.995147376310239196 ) ) ;
#10473=CARTESIAN_POINT ( 'NONE',  ( -92.62287095715005592, -23.47593901973091235, -1.443836447539002865 ) ) ;
#10474=CARTESIAN_POINT ( 'NONE',  ( -63.64766708060687250, -23.73791477778912196, 11.05961554403170766 ) ) ;
#10475=CARTESIAN_POINT ( 'NONE',  ( 19.74966320730700176, -10.79507447929251107, 11.49999999999999645 ) ) ;
#10476=ORIENTED_EDGE ( 'NONE', *, *, #68896, .T. ) ;
#10478=CARTESIAN_POINT ( 'NONE',  ( -21.86317675896206225, -2.224439152981679602, -1.500000000000002220 ) ) ;
#10479=CARTESIAN_POINT ( 'NONE',  ( -54.62287095715006302, -23.73907113216990439, -1.053371485793231921 ) ) ;
#10480=LINE ( 'NONE', #70386, #31670 ) ;
#10482=ORIENTED_EDGE ( 'NONE', *, *, #96079, .F. ) ;
#10483=FACE_OUTER_BOUND ( 'NONE', #25588, .T. ) ;
#10484=FACE_OUTER_BOUND ( 'NONE', #57597, .T. ) ;
#10486=CARTESIAN_POINT ( 'NONE',  ( -54.50803268341093144, -23.96169478059712787, 10.65365249895718947 ) ) ;
#10487=CARTESIAN_POINT ( 'NONE',  ( 1.819314030819549233, -20.42850443921780013, 11.49999999999998934 ) ) ;
#10489=ORIENTED_EDGE ( 'NONE', *, *, #27804, .F. ) ;
#10491=ORIENTED_EDGE ( 'NONE', *, *, #14791, .F. ) ;
#10492=ADVANCED_FACE ( 'NONE', ( #57877 ), #37390, .T. ) ;
#10493=CARTESIAN_POINT ( 'NONE',  ( -71.62287095715005592, -23.47593901973091235, -1.443836447539006196 ) ) ;
#10494=CARTESIAN_POINT ( 'NONE',  ( 22.67273400128462058, 4.441195646929153362, -1.500000000000002220 ) ) ;
#10495=CARTESIAN_POINT ( 'NONE',  ( -104.5495314845192496, -24.51419770103158768, 9.386484678747166299 ) ) ;
#10496=CARTESIAN_POINT ( 'NONE',  ( -20.10423522397153562, 3.301153050299447056, -1.500000000000002220 ) ) ;
#10497=ORIENTED_EDGE ( 'NONE', *, *, #40966, .T. ) ;
#10498=CARTESIAN_POINT ( 'NONE',  ( -71.37981187788743398, -25.12275311710066461, 7.103969935991345075 ) ) ;
#10500=CARTESIAN_POINT ( 'NONE',  ( -113.5228709571500616, -23.47593901973090524, -1.443836447538996204 ) ) ;
#10502=VERTEX_POINT ( 'NONE', #12167 ) ;
#10503=CARTESIAN_POINT ( 'NONE',  ( -108.8968792378191921, -29.50249817218807635, 6.986241424688308221 ) ) ;
#10504=CARTESIAN_POINT ( 'NONE',  ( -49.74369414166532977, -25.31573832230478516, 4.940877928549117115 ) ) ;
#10506=EDGE_LOOP ( 'NONE', ( #48416, #17574, #18828, #98353 ) ) ;
#10507=CARTESIAN_POINT ( 'NONE',  ( -12.88759680649768136, 16.30154091734715749, 11.49999999999998934 ) ) ;
#10508=EDGE_CURVE ( 'NONE', #67048, #85400, #58360, .T. ) ;
#10509=ORIENTED_EDGE ( 'NONE', *, *, #94259, .F. ) ;
#10510=CARTESIAN_POINT ( 'NONE',  ( -125.5894646780946999, -24.63355581998386512, 0.9682620441944075340 ) ) ;
#10511=ORIENTED_EDGE ( 'NONE', *, *, #36921, .F. ) ;
#10512=ADVANCED_FACE ( 'NONE', ( #53123 ), #88815, .F. ) ;
#10513=B_SPLINE_CURVE_WITH_KNOTS ( 'NONE', 3,
 ( #48365, #41249, #72205, #90411 ),
 .UNSPECIFIED., .F., .F.,
 ( 4, 4 ),
 ( 2.907410163773248763E-09, 0.002226547977040467356 ),
 .UNSPECIFIED. ) ;
#10514=CARTESIAN_POINT ( 'NONE',  ( -83.62287095715005592, -29.50250786944525672, 11.44777988621623521 ) ) ;
#10516=ORIENTED_EDGE ( 'NONE', *, *, #5204, .T. ) ;
#10520=B_SPLINE_CURVE_WITH_KNOTS ( 'NONE', 3,
 ( #10348, #80865, #41303, #72264, #30817, #2751, #11352, #33692 ),
 .UNSPECIFIED., .F., .F.,
 ( 4, 2, 2, 4 ),
 ( -0.001224873891641419573, -0.0002244903592271039420, 0.0007758931731872116891, 0.002776660238015838614 ),
 .UNSPECIFIED. ) ;
#10521=CARTESIAN_POINT ( 'NONE',  ( -46.52287095715006160, -23.48786465467241058, 11.44779295918255002 ) ) ;
#10522=CARTESIAN_POINT ( 'NONE',  ( 14.91618686576236108, -16.25093855066790738, 11.49999999999999645 ) ) ;
#10524=EDGE_CURVE ( 'NONE', #33210, #65583, #19281, .T. ) ;
#10525=CARTESIAN_POINT ( 'NONE',  ( -48.90936936008873914, -25.22646736291544656, 6.474846148537197976 ) ) ;
#10526=CARTESIAN_POINT ( 'NONE',  ( -22.11960324842224423, 4.537628740662121629, 11.49999999999998934 ) ) ;
#10527=EDGE_CURVE ( 'NONE', #66719, #36980, #84052, .T. ) ;
#10528=CARTESIAN_POINT ( 'NONE',  ( -101.1944152955115044, -29.50249789396666245, 6.858236616996303603 ) ) ;
#10529=ORIENTED_EDGE ( 'NONE', *, *, #76817, .T. ) ;
#10531=CARTESIAN_POINT ( 'NONE',  ( -93.55620429048339304, -23.47593901973091235, -1.443836447539002865 ) ) ;
#10532=VECTOR ( 'NONE', #36050, 1000.000000000000114 ) ;
#10533=CARTESIAN_POINT ( 'NONE',  ( -94.58953762381672448, -24.64898659630528854, 1.056161002820827699 ) ) ;
#10534=ORIENTED_EDGE ( 'NONE', *, *, #35129, .T. ) ;
#10535=CARTESIAN_POINT ( 'NONE',  ( -4.955175619359221351, 20.59750927568439138, 11.49999999999998934 ) ) ;
#10536=PLANE ( 'NONE',  #15739 ) ;
#10537=FACE_OUTER_BOUND ( 'NONE', #59261, .T. ) ;
#10540=CARTESIAN_POINT ( 'NONE',  ( 6.060481786824854389, 21.40074245971799627, -1.500000000000002220 ) ) ;
#10542=ORIENTED_EDGE ( 'NONE', *, *, #55328, .T. ) ;
#10544=CARTESIAN_POINT ( 'NONE',  ( -37.52763684613194783, -24.65952944569304250, 1.056160979905692576 ) ) ;
#10545=CARTESIAN_POINT ( 'NONE',  ( -16.37229413335033001, -10.43475415037859655, 11.49999999999999645 ) ) ;
#10547=CARTESIAN_POINT ( 'NONE',  ( -36.62904760676421745, -24.51419770103156637, 9.386484678747175181 ) ) ;
#10549=EDGE_CURVE ( 'NONE', #14489, #88666, #99754, .T. ) ;
#10550=CARTESIAN_POINT ( 'NONE',  ( -10.96721834449554933, 16.09610527815933168, 11.49999999999998934 ) ) ;
#10551=CARTESIAN_POINT ( 'NONE',  ( -15.65470850568805083, 14.63654280257262386, -1.500000000000002220 ) ) ;
#10552=CARTESIAN_POINT ( 'NONE',  ( -56.62287095715005592, -23.72747288104469376, -1.053458166803227014 ) ) ;
#10553=B_SPLINE_CURVE_WITH_KNOTS ( 'NONE', 3,
 ( #3072, #4566, #72085, #11167 ),
 .UNSPECIFIED., .F., .F.,
 ( 4, 4 ),
 ( 0.000000000000000000, 1.000000000000000000 ),
 .UNSPECIFIED. ) ;
#10556=CARTESIAN_POINT ( 'NONE',  ( -57.62287095715004881, -23.47593901973091235, -1.443836447539007972 ) ) ;
#10557=CARTESIAN_POINT ( 'NONE',  ( 12.47407908559008760, -19.03963781694049473, -1.500000000000002220 ) ) ;
#10559=CARTESIAN_POINT ( 'NONE',  ( -106.6235367854833243, -24.66019654487200441, 8.947790411086108620 ) ) ;
#10560=CARTESIAN_POINT ( 'NONE',  ( -73.52287095715007581, -23.47593901973090169, -1.443836447538996870 ) ) ;
#10561=CARTESIAN_POINT ( 'NONE',  ( 19.12242951303546334, 5.485007674754557527, 11.49999999999999645 ) ) ;
#10562=CARTESIAN_POINT ( 'NONE',  ( -78.62287095715005592, -24.64898659630367916, 1.056161002820826145 ) ) ;
#10563=CARTESIAN_POINT ( 'NONE',  ( -39.50522431325583739, -23.96169478059712787, 10.65365249895718769 ) ) ;
#10565=VERTEX_POINT ( 'NONE', #30258 ) ;
#10568=CARTESIAN_POINT ( 'NONE',  ( -15.38093110518717666, 15.28219592669002402, -1.500000000000002220 ) ) ;
#10569=CARTESIAN_POINT ( 'NONE',  ( -56.65739320408659552, -23.48786465467241413, 11.44779295918254647 ) ) ;
#10570=CARTESIAN_POINT ( 'NONE',  ( -12.57844902324429448, -14.85176824229388437, -1.500000000000002220 ) ) ;
#10571=DIRECTION ( 'NONE',  ( -3.773278334453080206E-23, 0.9999999999976377785, 2.173523156925979975E-06 ) ) ;
#10572=B_SPLINE_CURVE_WITH_KNOTS ( 'NONE', 3,
 ( #80755, #54539, #93582, #46425 ),
 .UNSPECIFIED., .F., .F.,
 ( 4, 4 ),
 ( 0.000000000000000000, 0.0001000000000000028644 ),
 .UNSPECIFIED. ) ;
#10576=CARTESIAN_POINT ( 'NONE',  ( 17.38039551199336685, -10.77953091123627694, 11.49999999999999645 ) ) ;
#10577=PLANE ( 'NONE',  #37530 ) ;
#10578=CARTESIAN_POINT ( 'NONE',  ( -118.6228709571500701, -23.48783264082478794, -1.443836473390058384 ) ) ;
#10579=EDGE_CURVE ( 'NONE', #44655, #52932, #60496, .T. ) ;
#10581=DIRECTION ( 'NONE',  ( 3.773278334444166432E-23, -1.000000000000000000, 0.000000000000000000 ) ) ;
#10586=FACE_OUTER_BOUND ( 'NONE', #19783, .T. ) ;
#10587=VERTEX_POINT ( 'NONE', #47501 ) ;
#10589=CARTESIAN_POINT ( 'NONE',  ( -66.55943436801386781, -23.73791477778911840, 11.05961554403170766 ) ) ;
#10590=EDGE_CURVE ( 'NONE', #99097, #13321, #53299, .T. ) ;
#10592=CARTESIAN_POINT ( 'NONE',  ( 17.95915693031428262, 14.28781372813260120, 11.49999999999999645 ) ) ;
#10593=CARTESIAN_POINT ( 'NONE',  ( 7.803535043518188274, -21.38454823780343617, 11.49999999999998934 ) ) ;
#10595=CARTESIAN_POINT ( 'NONE',  ( -75.62287095715007013, -23.85229601348995132, 10.88205029486209163 ) ) ;
#10596=CARTESIAN_POINT ( 'NONE',  ( -90.50112360221751828, -24.83618233451451118, 1.606449574219535492 ) ) ;
#10599=CARTESIAN_POINT ( 'NONE',  ( -69.34917151123886470, -25.24288101849653998, 6.331981848628771559 ) ) ;
#10601=CARTESIAN_POINT ( 'NONE',  ( 8.256513476402210117, 20.27555108428041208, -1.500000000000002220 ) ) ;
#10602=CARTESIAN_POINT ( 'NONE',  ( -69.58050984181491572, -24.66019654487199375, 8.947790411086119278 ) ) ;
#10604=B_SPLINE_CURVE_WITH_KNOTS ( 'NONE', 3,
 ( #84594, #32311, #69374, #70888, #30304, #77963 ),
 .UNSPECIFIED., .F., .F.,
 ( 4, 2, 4 ),
 ( 0.000000000000000000, 0.001380764517854766050, 0.002761529035709532100 ),
 .UNSPECIFIED. ) ;
#10605=CARTESIAN_POINT ( 'NONE',  ( -48.87380231474225667, -25.26256937810135028, 6.137091986423513390 ) ) ;
#10606=CARTESIAN_POINT ( 'NONE',  ( -71.69009546357753493, -25.26814388089136187, 5.957693125896286190 ) ) ;
#10607=CARTESIAN_POINT ( 'NONE',  ( -99.16166289166534398, -25.25460552112298984, 5.311370849885090450 ) ) ;
#10608=ORIENTED_EDGE ( 'NONE', *, *, #13103, .T. ) ;
#10609=CARTESIAN_POINT ( 'NONE',  ( -19.37329759448073574, 6.469241145865432863, 11.49999999999998934 ) ) ;
#10610=ORIENTED_EDGE ( 'NONE', *, *, #67090, .T. ) ;
#10611=VECTOR ( 'NONE', #56737, 1000.000000000000000 ) ;
#10614=EDGE_CURVE ( 'NONE', #87028, #17763, #12132, .T. ) ;
#10616=CARTESIAN_POINT ( 'NONE',  ( 22.26416322464526232, -5.798680748638591176, 11.49999999999998934 ) ) ;
#10620=CARTESIAN_POINT ( 'NONE',  ( -108.5200640884878283, -23.73791477778912196, 11.05961554403169878 ) ) ;
#10621=CARTESIAN_POINT ( 'NONE',  ( -48.52287095715006870, -23.96177878511308634, 10.65340807706329862 ) ) ;
#10623=EDGE_CURVE ( 'NONE', #94697, #76683, #31262, .T. ) ;
#10625=CARTESIAN_POINT ( 'NONE',  ( -117.0509084556500881, -25.24723402497068037, 6.200314804519077683 ) ) ;
#10626=CARTESIAN_POINT ( 'NONE',  ( -20.51402961445061734, 6.013860829077147585, 11.49999999999999645 ) ) ;
#10628=ORIENTED_EDGE ( 'NONE', *, *, #39112, .F. ) ;
#10629=CARTESIAN_POINT ( 'NONE',  ( -10.71655374829924767, -19.46388382022006525, -1.500000000000002220 ) ) ;
#10630=CARTESIAN_POINT ( 'NONE',  ( 12.06641648444584369, 16.80774221200798735, 11.49999999999998934 ) ) ;
#10632=ORIENTED_EDGE ( 'NONE', *, *, #47073, .F. ) ;
#10636=DIRECTION ( 'NONE',  ( -3.773278334453079618E-23, 0.9999999999976377785, 2.173523156925979975E-06 ) ) ;
#10637=ORIENTED_EDGE ( 'NONE', *, *, #89330, .F. ) ;
#10638=CARTESIAN_POINT ( 'NONE',  ( -50.38191529551148307, -25.27517877397642110, 2.832404459008946773 ) ) ;
#10640=CARTESIAN_POINT ( 'NONE',  ( -0.7727808018759799724, -20.89725122839497828, -1.500000000000002220 ) ) ;
#10641=CARTESIAN_POINT ( 'NONE',  ( -21.85961425739535358, 0.8689724601130633941, 11.49999999999999645 ) ) ;
#10642=ADVANCED_FACE ( 'NONE', ( #53624 ), #70836, .T. ) ;
#10643=CARTESIAN_POINT ( 'NONE',  ( -26.43901205547898670, -24.89279823874531061, 6.777242086831815726 ) ) ;
#10644=FACE_OUTER_BOUND ( 'NONE', #32842, .T. ) ;
#10645=CARTESIAN_POINT ( 'NONE',  ( 3.433349652534986696, 22.22849440524942111, 11.49999999999998934 ) ) ;
#10646=CARTESIAN_POINT ( 'NONE',  ( -17.10473743203234775, -12.04273770408705246, 11.49999999999998934 ) ) ;
#10648=CARTESIAN_POINT ( 'NONE',  ( -38.60080910673752896, -23.96119346886880308, -0.6495511937831990323 ) ) ;
#10650=CARTESIAN_POINT ( 'NONE',  ( -44.62287095715004881, -23.47593901973091235, -1.443836447539011525 ) ) ;
#10651=ORIENTED_EDGE ( 'NONE', *, *, #23665, .F. ) ;
#10655=ORIENTED_EDGE ( 'NONE', *, *, #97357, .F. ) ;
#10656=CARTESIAN_POINT ( 'NONE',  ( -99.33919073176147663, -25.12215527841457785, 6.423374680119191993 ) ) ;
#10657=ORIENTED_EDGE ( 'NONE', *, *, #17962, .F. ) ;
#10658=B_SPLINE_CURVE_WITH_KNOTS ( 'NONE', 3,
 ( #95355, #89747, #33958, #42587 ),
 .UNSPECIFIED., .F., .F.,
 ( 4, 4 ),
 ( 0.5208719419040093168, 0.5298783731761248506 ),
 .UNSPECIFIED. ) ;
#10659=CARTESIAN_POINT ( 'NONE',  ( 0.5228555243449846124, 21.43159495547403282, -1.500000000000002220 ) ) ;
#10660=EDGE_LOOP ( 'NONE', ( #28962, #46528, #100186, #93501 ) ) ;
#10662=CARTESIAN_POINT ( 'NONE',  ( 10.44912437418449969, 18.32051524777507723, 11.49999999999998934 ) ) ;
#10663=CARTESIAN_POINT ( 'NONE',  ( -30.59475437726466751, -24.84008585880724596, 8.370654131274084975 ) ) ;
#10664=CARTESIAN_POINT ( 'NONE',  ( -127.4728709571500360, -25.40558663563398767, 5.000950440326727531 ) ) ;
#10666=CARTESIAN_POINT ( 'NONE',  ( -101.6292215989844721, -24.15543982623907482, -0.2315651400026588480 ) ) ;
#10668=CARTESIAN_POINT ( 'NONE',  ( 6.148021820315829444, -21.18842874637755358, -1.500000000000002220 ) ) ;
#10669=ORIENTED_EDGE ( 'NONE', *, *, #92593, .T. ) ;
#10670=CARTESIAN_POINT ( 'NONE',  ( -116.6285100755955426, -23.73766607897671577, -1.055555164236427590 ) ) ;
#10672=CARTESIAN_POINT ( 'NONE',  ( -40.63161819696095733, -25.31624740998290335, 5.540357839096273551 ) ) ;
#10673=CARTESIAN_POINT ( 'NONE',  ( -62.55964932266956424, -23.73791477778911840, 11.05961554403171121 ) ) ;
#10674=B_SPLINE_CURVE_WITH_KNOTS ( 'NONE', 3,
 ( #98546, #28059, #89949, #58518 ),
 .UNSPECIFIED., .F., .F.,
 ( 4, 4 ),
 ( 0.8593950407724427754, 0.8603957878132079129 ),
 .UNSPECIFIED. ) ;
#10675=FACE_OUTER_BOUND ( 'NONE', #64975, .T. ) ;
#10676=CARTESIAN_POINT ( 'NONE',  ( -38.62287095715005592, -23.48786465467240703, 11.44779295918255180 ) ) ;
#10677=CARTESIAN_POINT ( 'NONE',  ( -18.83571791729191958, -9.990160686573538840, 11.49999999999998934 ) ) ;
#10678=DIRECTION ( 'NONE',  ( -1.000000000000000000, -3.773278334444167608E-23, -8.201307833595939069E-29 ) ) ;
#10679=CARTESIAN_POINT ( 'NONE',  ( -50.61388679491238918, -25.19715874454066906, 3.309015525357478893 ) ) ;
#10681=CARTESIAN_POINT ( 'NONE',  ( -81.45492590815939593, -25.22427035087299174, 6.407323222939080409 ) ) ;
#10682=CARTESIAN_POINT ( 'NONE',  ( 18.83488669200175281, -12.41447709603701632, -1.500000000000002220 ) ) ;
#10685=ORIENTED_EDGE ( 'NONE', *, *, #40937, .F. ) ;
#10686=VECTOR ( 'NONE', #99244, 1000.000000000000114 ) ;
#10688=CARTESIAN_POINT ( 'NONE',  ( -67.62287095715005592, -23.47593901973091235, -1.443836447539006196 ) ) ;
#10689=CARTESIAN_POINT ( 'NONE',  ( -19.65353550717971487, 1.628721094194526486, 11.49999999999999645 ) ) ;
#10690=CARTESIAN_POINT ( 'NONE',  ( -38.62287095715005592, -29.50250243563736774, 8.947779886222148704 ) ) ;
#10692=CARTESIAN_POINT ( 'NONE',  ( -67.60279521098367184, -23.73766607897670511, -1.055555164236457788 ) ) ;
#10693=ORIENTED_EDGE ( 'NONE', *, *, #12994, .F. ) ;
#10695=CARTESIAN_POINT ( 'NONE',  ( -117.5562042904833788, -24.65952944569305316, 1.056160979905707009 ) ) ;
#10696=FACE_OUTER_BOUND ( 'NONE', #69239, .T. ) ;
#10698=CARTESIAN_POINT ( 'NONE',  ( -90.62287095715004170, -23.47593901973091235, -1.443836447539002865 ) ) ;
#10701=CARTESIAN_POINT ( 'NONE',  ( -109.6228709571500417, -23.48783264082478794, -1.443836473390060382 ) ) ;
#10702=CARTESIAN_POINT ( 'NONE',  ( -81.67165532884091306, -25.16133908214882808, 6.940091796881004527 ) ) ;
#10703=CARTESIAN_POINT ( 'NONE',  ( -10.52764212615999639, 16.74383705166681580, 11.49999999999998934 ) ) ;
#10705=CARTESIAN_POINT ( 'NONE',  ( 20.19498477198788322, 0.2509159868347127231, 11.49999999999999645 ) ) ;
#10707=B_SPLINE_CURVE_WITH_KNOTS ( 'NONE', 3,
 ( #22665, #21180, #44534, #14568 ),
 .UNSPECIFIED., .F., .F.,
 ( 4, 4 ),
 ( 0.7610434424937544406, 0.7700498737658699744 ),
 .UNSPECIFIED. ) ;
#10713=ADVANCED_FACE ( 'NONE', ( #92654 ), #71338, .T. ) ;
#10714=CARTESIAN_POINT ( 'NONE',  ( -39.62287095715006302, -23.73907113216990439, -1.053371485793234807 ) ) ;
#10716=CARTESIAN_POINT ( 'NONE',  ( -58.62287095715004881, -24.64898659630367916, 1.056161002820822592 ) ) ;
#10717=CARTESIAN_POINT ( 'NONE',  ( 20.02521558760690112, -0.9251608499524575091, 11.49999999999998934 ) ) ;
#10718=ADVANCED_FACE ( 'NONE', ( #88064 ), #88563, .F. ) ;
#10719=DIRECTION ( 'NONE',  ( -3.773278334444166432E-23, 1.000000000000000000, 0.000000000000000000 ) ) ;
#10723=CARTESIAN_POINT ( 'NONE',  ( -103.5228709571500758, -24.35013146730203815, 9.818937971375097717 ) ) ;
#10724=CARTESIAN_POINT ( 'NONE',  ( -35.63737625694447786, -24.63355581998387223, 0.9682620441943878831 ) ) ;
#10725=CARTESIAN_POINT ( 'NONE',  ( -79.62287095715005592, -29.50248528299804818, 1.056150453629038477 ) ) ;
#10727=CARTESIAN_POINT ( 'NONE',  ( -101.2039755539695136, -25.14901327759760719, 3.054686125765971205 ) ) ;
#10728=CARTESIAN_POINT ( 'NONE',  ( -40.41683116089613748, -29.50249403413438642, 5.082395270846652657 ) ) ;
#10729=CARTESIAN_POINT ( 'NONE',  ( -100.9381932429152045, -25.20650842489795807, 6.812665538484691474 ) ) ;
#10731=CARTESIAN_POINT ( 'NONE',  ( -15.63206872509828571, 12.99414084278249071, 11.49999999999998934 ) ) ;
#10734=CARTESIAN_POINT ( 'NONE',  ( -32.63552282000483018, -24.34968618360933590, 0.1864209137778856384 ) ) ;
#10735=CARTESIAN_POINT ( 'NONE',  ( -127.5212380171430198, -24.35071581493544102, 9.817618358456009275 ) ) ;
#10737=FACE_OUTER_BOUND ( 'NONE', #67519, .T. ) ;
#10741=CARTESIAN_POINT ( 'NONE',  ( -30.47287095715007510, -24.67069026960422562, 8.894128854304588216 ) ) ;
#10742=CARTESIAN_POINT ( 'NONE',  ( 19.29917393477590437, 8.764703196630867055, 11.49999999999999645 ) ) ;
#10743=CARTESIAN_POINT ( 'NONE',  ( 21.88104185797606505, 3.448541436957560880, -1.500000000000002220 ) ) ;
#10744=CARTESIAN_POINT ( 'NONE',  ( 3.086129920417311823, 20.35385046113321295, -1.500000000000002220 ) ) ;
#10747=CARTESIAN_POINT ( 'NONE',  ( -94.52287095715007581, -24.51387760970725083, 9.387446482453412955 ) ) ;
#10749=DIRECTION ( 'NONE',  ( -3.773278334453079618E-23, 0.9999999999976377785, 2.173523156925979975E-06 ) ) ;
#10750=CARTESIAN_POINT ( 'NONE',  ( -50.52287095715006870, -24.14406661686760458, 10.28769366194083013 ) ) ;
#10751=VERTEX_POINT ( 'NONE', #49510 ) ;
#10755=CARTESIAN_POINT ( 'NONE',  ( -83.62287095715004170, -23.96127896941632685, -0.6493128931037841500 ) ) ;
#10757=CARTESIAN_POINT ( 'NONE',  ( -91.62287095715004170, -23.73907113216990794, -1.053371485793224149 ) ) ;
#10758=CARTESIAN_POINT ( 'NONE',  ( 8.970943996638910178, -18.66293075132952950, -1.500000000000002220 ) ) ;
#10760=CARTESIAN_POINT ( 'NONE',  ( -7.614213781628100364, -20.28429660096114517, 11.49999999999999645 ) ) ;
#10763=CARTESIAN_POINT ( 'NONE',  ( -110.7042636268849094, -25.11831750865088964, 2.876796822534068987 ) ) ;
#10764=CARTESIAN_POINT ( 'NONE',  ( 21.53444271425275858, 6.169869319618734416, 11.49999999999998934 ) ) ;
#10765=EDGE_CURVE ( 'NONE', #77504, #40376, #15723, .T. ) ;
#10768=ORIENTED_EDGE ( 'NONE', *, *, #64578, .T. ) ;
#10769=CARTESIAN_POINT ( 'NONE',  ( -45.55620429048339304, -24.99132157543166599, 2.256160258750668390 ) ) ;
#10770=CARTESIAN_POINT ( 'NONE',  ( -85.58953762381673869, -24.99132157543083821, 2.256160258750495640 ) ) ;
#10771=ORIENTED_EDGE ( 'NONE', *, *, #24341, .F. ) ;
#10772=ORIENTED_EDGE ( 'NONE', *, *, #13099, .F. ) ;
#10773=EDGE_CURVE ( 'NONE', #85117, #65926, #6023, .T. ) ;
#10774=CARTESIAN_POINT ( 'NONE',  ( -103.6228709571500701, -24.33832256526969928, 0.1851278514119971963 ) ) ;
#10776=DIRECTION ( 'NONE',  ( 0.000000000000000000, -0.9999999999976377785, -2.173523156925979975E-06 ) ) ;
#10777=CARTESIAN_POINT ( 'NONE',  ( -3.310264809446246570, -21.00426241492911927, -1.500000000000002220 ) ) ;
#10778=ORIENTED_EDGE ( 'NONE', *, *, #12249, .T. ) ;
#10779=CARTESIAN_POINT ( 'NONE',  ( -100.4426124108961176, -25.12298712672051337, 7.101635559041870494 ) ) ;
#10780=CARTESIAN_POINT ( 'NONE',  ( -6.457742198559264679, -20.83860622980983024, 11.49999999999998934 ) ) ;
#10781=CARTESIAN_POINT ( 'NONE',  ( -52.50174715697038152, -24.15620529776627734, 10.23563542870661180 ) ) ;
#10784=CARTESIAN_POINT ( 'NONE',  ( 21.76694381678408519, 2.417257996116004115, -1.500000000000002220 ) ) ;
#10785=CARTESIAN_POINT ( 'NONE',  ( -66.62287095715005592, -24.65952944569304606, 1.056160979905696573 ) ) ;
#10788=CARTESIAN_POINT ( 'NONE',  ( -85.58736961604824955, -24.63419186844611275, 9.035850630976915099 ) ) ;
#10792=ORIENTED_EDGE ( 'NONE', *, *, #19017, .T. ) ;
#10793=FACE_OUTER_BOUND ( 'NONE', #43817, .T. ) ;
#10794=CARTESIAN_POINT ( 'NONE',  ( -31.24388727629347073, -25.31501645218191143, 6.103840189645985070 ) ) ;
#10795=CARTESIAN_POINT ( 'NONE',  ( -3.247986963444697395, 20.98610878802851332, 11.49999999999998934 ) ) ;
#10797=CARTESIAN_POINT ( 'NONE',  ( -130.5728709571500588, -24.93418366566758948, 8.369064737642425200 ) ) ;
#10798=CARTESIAN_POINT ( 'NONE',  ( -100.4426124108961176, -25.12298712672051337, 7.101635559041870494 ) ) ;
#10799=CARTESIAN_POINT ( 'NONE',  ( -68.59250847563207287, -24.15543982623907127, -0.2315651400026649820 ) ) ;
#10800=CARTESIAN_POINT ( 'NONE',  ( 13.61561175257155298, 13.87280521877887018, -1.500000000000002220 ) ) ;
#10801=CARTESIAN_POINT ( 'NONE',  ( -45.60108961187481214, -24.15503026093915651, -0.2815557561904415418 ) ) ;
#10803=CARTESIAN_POINT ( 'NONE',  ( -13.79594968651775666, -13.80015156857029268, 11.49999999999999645 ) ) ;
#10805=CARTESIAN_POINT ( 'NONE',  ( -68.52287095715006160, -24.64898659630528854, 1.056161002820824368 ) ) ;
#10806=ORIENTED_EDGE ( 'NONE', *, *, #37843, .F. ) ;
#10808=FACE_OUTER_BOUND ( 'NONE', #65025, .T. ) ;
#10810=CARTESIAN_POINT ( 'NONE',  ( -51.55620429048339304, -23.48783264082478084, -1.443836473390070152 ) ) ;
#10811=CARTESIAN_POINT ( 'NONE',  ( -80.89908437845683409, -25.03156050640678743, 7.516075442759441394 ) ) ;
#10812=CARTESIAN_POINT ( 'NONE',  ( -15.16924259816527609, 12.53091941037558854, 11.49999999999998934 ) ) ;
#10815=CARTESIAN_POINT ( 'NONE',  ( 19.36532470938277228, 12.59445105952145738, -1.500000000000002220 ) ) ;
#10821=CARTESIAN_POINT ( 'NONE',  ( -92.62287095715009855, -23.73907113216991505, -1.053371485793224371 ) ) ;
#10822=CARTESIAN_POINT ( 'NONE',  ( -105.6228709571499991, -24.63345952396255711, 9.038047939301501188 ) ) ;
#10824=AXIS2_PLACEMENT_3D ( 'NONE', #12368, #81893, #27614 ) ;
#10826=AXIS2_PLACEMENT_3D ( 'NONE', #64211, #26629, #25623 ) ;
#10828=CARTESIAN_POINT ( 'NONE',  ( -73.52287095715013265, -24.33832256527049154, 0.1851278514138621212 ) ) ;
#10829=CARTESIAN_POINT ( 'NONE',  ( 16.79105032741591330, -10.77411451815220822, -1.500000000000002220 ) ) ;
#10831=CARTESIAN_POINT ( 'NONE',  ( -47.52287095715006160, -29.50248528299804818, 1.056150453629033370 ) ) ;
#10832=CARTESIAN_POINT ( 'NONE',  ( 12.47747183659840786, 15.48776231947736015, -1.500000000000002220 ) ) ;
#10835=CARTESIAN_POINT ( 'NONE',  ( -89.81226385320383088, -25.27367468601175204, 3.993462154588550916 ) ) ;
#10836=ADVANCED_FACE ( 'NONE', ( #25145 ), #6837, .T. ) ;
#10837=ADVANCED_FACE ( 'NONE', ( #21519 ), #58611, .T. ) ;
#10838=DIRECTION ( 'NONE',  ( 3.773278334444166432E-23, -1.000000000000000000, 0.000000000000000000 ) ) ;
#10840=CARTESIAN_POINT ( 'NONE',  ( -80.57997149293382222, -25.00182538069147142, 7.747789668545041586 ) ) ;
#10841=CARTESIAN_POINT ( 'NONE',  ( -11.59579830748209517, 17.24510332420730663, 11.49999999999999645 ) ) ;
#10843=EDGE_CURVE ( 'NONE', #77757, #79556, #84734, .T. ) ;
#10845=CARTESIAN_POINT ( 'NONE',  ( -19.58686714514938387, 11.73587220785771379, 11.49999999999999645 ) ) ;
#10849=ORIENTED_EDGE ( 'NONE', *, *, #94370, .T. ) ;
#10850=CARTESIAN_POINT ( 'NONE',  ( 14.48468284575590204, 14.13777120147990729, -1.500000000000002220 ) ) ;
#10851=CARTESIAN_POINT ( 'NONE',  ( -106.5228709571501469, -23.96177878511310055, 10.65340807706329507 ) ) ;
#10854=EDGE_CURVE ( 'NONE', #31528, #7274, #7275, .T. ) ;
#10855=CARTESIAN_POINT ( 'NONE',  ( -50.55620429048339304, -23.48786465467240703, 11.44779295918255357 ) ) ;
#10857=CARTESIAN_POINT ( 'NONE',  ( -105.6228709571500559, -23.47596703998600631, 11.44779298504227860 ) ) ;
#10859=CARTESIAN_POINT ( 'NONE',  ( 18.25133680241413359, 8.160682379734268466, -1.500000000000002220 ) ) ;
#10860=CARTESIAN_POINT ( 'NONE',  ( 15.04517842881462819, -14.58609674458608829, 11.49999999999999645 ) ) ;
#10862=CARTESIAN_POINT ( 'NONE',  ( -28.07643796139391057, -24.68838396948798319, 8.218772173470371811 ) ) ;
#10863=CARTESIAN_POINT ( 'NONE',  ( -93.52287095715006160, -23.48786465467241769, 11.44779295918254292 ) ) ;
#10864=CARTESIAN_POINT ( 'NONE',  ( 7.103389721457689099, 20.86620700561973862, 11.49999999999998934 ) ) ;
#10865=CARTESIAN_POINT ( 'NONE',  ( -39.78092788824959314, -25.27806063382736568, 4.883081681052058975 ) ) ;
#10866=EDGE_LOOP ( 'NONE', ( #79703, #91468, #23348, #59026 ) ) ;
#10868=CARTESIAN_POINT ( 'NONE',  ( -88.62287095715004170, -29.50248528299804818, 1.056150453629040253 ) ) ;
#10870=ORIENTED_EDGE ( 'NONE', *, *, #87243, .T. ) ;
#10871=DIRECTION ( 'NONE',  ( 3.773278334444167608E-23, -1.000000000000000000, 0.000000000000000000 ) ) ;
#10872=ORIENTED_EDGE ( 'NONE', *, *, #22489, .F. ) ;
#10875=FACE_OUTER_BOUND ( 'NONE', #96007, .T. ) ;
#10876=CARTESIAN_POINT ( 'NONE',  ( -91.15361000704997707, -25.26877915520014639, 5.947789088310639904 ) ) ;
#10877=CARTESIAN_POINT ( 'NONE',  ( 1.819314030819549233, -20.42850443921780013, -1.500000000000002220 ) ) ;
#10879=CARTESIAN_POINT ( 'NONE',  ( -49.27932720226401386, -25.25530279399480449, 6.214150124083338333 ) ) ;
#10882=CARTESIAN_POINT ( 'NONE',  ( 15.82088602905085750, -15.72875506571707760, 11.49999999999998934 ) ) ;
#10885=CARTESIAN_POINT ( 'NONE',  ( -104.5895376238167245, -24.64898659630529210, 1.056161002820830142 ) ) ;
#10886=ORIENTED_EDGE ( 'NONE', *, *, #93173, .T. ) ;
#10889=CARTESIAN_POINT ( 'NONE',  ( -17.86878485216894319, -10.78119150571587781, -1.500000000000002220 ) ) ;
#10892=DIRECTION ( 'NONE',  ( -3.773278334453079030E-23, 0.9999999999976377785, 2.173523156925979128E-06 ) ) ;
#10893=ORIENTED_EDGE ( 'NONE', *, *, #39107, .F. ) ;
#10894=AXIS2_PLACEMENT_3D ( 'NONE', #31314, #46547, #39434 ) ;
#10895=VERTEX_POINT ( 'NONE', #75812 ) ;
#10897=CARTESIAN_POINT ( 'NONE',  ( -5.295558097854481616, 20.35707381486366785, -1.500000000000002220 ) ) ;
#10899=ORIENTED_EDGE ( 'NONE', *, *, #96526, .T. ) ;
#10902=CARTESIAN_POINT ( 'NONE',  ( -120.5896284256728990, -24.52399227489125266, 9.353111116836528183 ) ) ;
#10904=CARTESIAN_POINT ( 'NONE',  ( -101.2262178754702120, -25.03152408370649340, 7.375461323086289767 ) ) ;
#10905=CARTESIAN_POINT ( 'NONE',  ( -129.6228709571500701, -23.95044443724993144, 10.65354141964649948 ) ) ;
#10906=CARTESIAN_POINT ( 'NONE',  ( 18.84366469573077296, 10.75509914293975555, -1.500000000000002220 ) ) ;
#10907=CARTESIAN_POINT ( 'NONE',  ( -80.94627791849588050, -25.24759782953908527, 7.000535489368433062 ) ) ;
#10908=CARTESIAN_POINT ( 'NONE',  ( 7.309977242446557888, -21.02818303981469583, 11.49999999999999645 ) ) ;
#10909=ORIENTED_EDGE ( 'NONE', *, *, #69008, .T. ) ;
#10910=CARTESIAN_POINT ( 'NONE',  ( -51.19842764437002813, -25.24728787901509008, 5.493892441256813974 ) ) ;
#10912=EDGE_CURVE ( 'NONE', #11878, #39724, #37267, .T. ) ;
#10913=CARTESIAN_POINT ( 'NONE',  ( -70.41980003698678559, -25.30157081653178608, 5.314949076439312137 ) ) ;
#10915=LINE ( 'NONE', #57105, #53908 ) ;
#10916=VERTEX_POINT ( 'NONE', #12422 ) ;
#10917=ORIENTED_EDGE ( 'NONE', *, *, #89712, .F. ) ;
#10923=CARTESIAN_POINT ( 'NONE',  ( -130.5728709571500872, -24.61548261799620363, 0.6545881806958654403 ) ) ;
#10924=CARTESIAN_POINT ( 'NONE',  ( -11.68221627493902126, 19.09626523228051553, -1.500000000000002220 ) ) ;
#10926=CARTESIAN_POINT ( 'NONE',  ( -112.5587162177321972, -23.48786465467241769, 11.44779295918253936 ) ) ;
#10927=CARTESIAN_POINT ( 'NONE',  ( -101.5603781230100680, -23.48786465467241413, 11.44779295918254469 ) ) ;
#10928=CARTESIAN_POINT ( 'NONE',  ( -39.44687923781921057, -25.28830591450888221, 4.188173661249233959 ) ) ;
#10930=CARTESIAN_POINT ( 'NONE',  ( -54.62287095715005592, -24.64898659630528854, 1.056161002820821038 ) ) ;
#10931=CARTESIAN_POINT ( 'NONE',  ( -97.25305430158761055, -24.26827793580486059, 9.960784317162948653 ) ) ;
#10932=CARTESIAN_POINT ( 'NONE',  ( 14.99095386781537975, 12.61000069877385421, -1.500000000000002220 ) ) ;
#10933=B_SPLINE_SURFACE_WITH_KNOTS ( 'NONE', 3, 3, ( 
 ( #67236, #76801, #45392, #51998 ),
 ( #98149, #28163, #37764, #68721 ),
 ( #37270, #68222, #66748, #99149 ),
 ( #53509, #98651, #61115, #29649 ),
 ( #82436, #21029, #99639, #82929 ),
 ( #45886, #75318, #13417, #5813 ),
 ( #60122, #60623, #36276, #84432 ) ),
 .UNSPECIFIED., .F., .F., .F.,
 ( 4, 3, 4 ),
 ( 4, 4 ),
 ( 0.7945040050992252523, 0.8970133687736511208, 0.9995227324480769893 ),
 ( 0.9697404217223760670, 0.9712008428071842170 ),
 .UNSPECIFIED. ) ;
#10935=ORIENTED_EDGE ( 'NONE', *, *, #29623, .F. ) ;
#10936=CARTESIAN_POINT ( 'NONE',  ( -5.740839400147730309, 20.75665450205591966, -1.500000000000002220 ) ) ;
#10938=CARTESIAN_POINT ( 'NONE',  ( -128.5213307013914630, -24.65952944569305316, 1.056160979905708341 ) ) ;
#10939=B_SPLINE_CURVE_WITH_KNOTS ( 'NONE', 3,
 ( #8649, #77640, #93877, #53331, #99477, #45215, #77139, #76141 ),
 .UNSPECIFIED., .F., .F.,
 ( 4, 2, 2, 4 ),
 ( 6.391158118962920407E-06, 0.002007136338672923116, 0.003007508928949902995, 0.004007881519226883307 ),
 .UNSPECIFIED. ) ;
#10940=CARTESIAN_POINT ( 'NONE',  ( -71.30218710724507503, -25.12218970343873536, 6.299238622824248068 ) ) ;
#10941=CARTESIAN_POINT ( 'NONE',  ( -63.55620429048339304, -24.66019654487199020, 8.947790411086131712 ) ) ;
#10942=CARTESIAN_POINT ( 'NONE',  ( -82.52287095715006160, -24.65952944569304606, 1.056160979905698794 ) ) ;
#10943=B_SPLINE_CURVE_WITH_KNOTS ( 'NONE', 3,
 ( #73595, #36019, #4085, #74581, #43152, #68968, #83183, #46141 ),
 .UNSPECIFIED., .F., .F.,
 ( 4, 2, 2, 4 ),
 ( 6.391158118963016122E-06, 0.002007136338672923983, 0.003007508928949904729, 0.004007881519226885042 ),
 .UNSPECIFIED. ) ;
#10944=CARTESIAN_POINT ( 'NONE',  ( 22.25235761598246143, -5.642936543268669780, -1.500000000000002220 ) ) ;
#10947=CARTESIAN_POINT ( 'NONE',  ( -49.51416547925957445, -23.73766607897670156, -1.055555164236457566 ) ) ;
#10948=CARTESIAN_POINT ( 'NONE',  ( -5.826506878040391690, 19.21762618028343184, 11.49999999999999645 ) ) ;
#10949=CARTESIAN_POINT ( 'NONE',  ( -110.0261373028301080, -25.10927401252845925, 2.855322574578669670 ) ) ;
#10952=CARTESIAN_POINT ( 'NONE',  ( -113.6228709571500417, -23.48783264082479150, -1.443836473390060160 ) ) ;
#10954=CARTESIAN_POINT ( 'NONE',  ( -18.24533751216517885, 7.751685665592884078, -1.500000000000002220 ) ) ;
#10956=CARTESIAN_POINT ( 'NONE',  ( -16.05533900033903549, 11.45903963230415101, -1.500000000000002220 ) ) ;
#10963=CARTESIAN_POINT ( 'NONE',  ( 19.85042311639309531, 5.490197614093233369, 11.49999999999999645 ) ) ;
#10967=CARTESIAN_POINT ( 'NONE',  ( -6.441999407266626676, 21.70310835763521595, 11.49999999999999645 ) ) ;
#10969=CARTESIAN_POINT ( 'NONE',  ( -69.70298246041917878, -25.12219101354323669, 6.901994799867971153 ) ) ;
#10970=CARTESIAN_POINT ( 'NONE',  ( -97.51896588966310730, -23.73766607897671221, -1.055555164236451793 ) ) ;
#10971=VECTOR ( 'NONE', #64615, 1000.000000000000114 ) ;
#10972=EDGE_CURVE ( 'NONE', #34090, #40854, #89595, .T. ) ;
#10973=CARTESIAN_POINT ( 'NONE',  ( -27.55559746109228669, -24.93063634460818889, 8.249644825981562235 ) ) ;
#10975=B_SPLINE_CURVE_WITH_KNOTS ( 'NONE', 3,
 ( #26697, #71880, #87088, #41935, #95207, #72379 ),
 .UNSPECIFIED., .F., .F.,
 ( 4, 2, 4 ),
 ( 0.000000000000000000, 0.001380901958385388545, 0.002761803916770777089 ),
 .UNSPECIFIED. ) ;
#10976=ORIENTED_EDGE ( 'NONE', *, *, #21336, .T. ) ;
#10977=CARTESIAN_POINT ( 'NONE',  ( -79.34772585426964042, -25.31596430212281135, 5.924311783118726638 ) ) ;
#10978=CARTESIAN_POINT ( 'NONE',  ( -15.12447472116105729, 17.10960193589383849, 11.49999999999998934 ) ) ;
#10980=FACE_OUTER_BOUND ( 'NONE', #20904, .T. ) ;
#10981=CARTESIAN_POINT ( 'NONE',  ( -82.63662447401794964, -23.96169478059713143, 10.65365249895718414 ) ) ;
#10982=CARTESIAN_POINT ( 'NONE',  ( 21.16529133594374557, -7.503415950508986576, 11.49999999999999645 ) ) ;
#10984=CARTESIAN_POINT ( 'NONE',  ( -36.52287095715006870, -23.47596703998600631, 11.44779298504229281 ) ) ;
#10985=CARTESIAN_POINT ( 'NONE',  ( 15.04091035147580335, -15.99806323810862274, -1.500000000000002220 ) ) ;
#10986=CARTESIAN_POINT ( 'NONE',  ( -127.4336609825043070, -25.40057329150818077, 4.607792141311833234 ) ) ;
#10987=CARTESIAN_POINT ( 'NONE',  ( -44.61594382116558677, -23.48786465467240347, 11.44779295918255180 ) ) ;
#10988=CARTESIAN_POINT ( 'NONE',  ( -118.5228709571501184, -23.48783264082477373, -1.443836473390083475 ) ) ;
#10991=CARTESIAN_POINT ( 'NONE',  ( -111.6228709571500559, -23.72747288104441665, -1.053458166803660889 ) ) ;
#10993=CARTESIAN_POINT ( 'NONE',  ( -45.52287095715004739, -24.82558206586142902, 1.605769216559445933 ) ) ;
#10994=CARTESIAN_POINT ( 'NONE',  ( 7.908618202329199320, -18.92053725880622039, -1.500000000000002220 ) ) ;
#10998=ORIENTED_EDGE ( 'NONE', *, *, #26175, .T. ) ;
#10999=CARTESIAN_POINT ( 'NONE',  ( -61.62287095715004881, -29.50247984919015209, -1.443849546365056913 ) ) ;
#11000=CARTESIAN_POINT ( 'NONE',  ( 11.81885653190370888, -19.86314957129924608, 11.49999999999998934 ) ) ;
#11001=CARTESIAN_POINT ( 'NONE',  ( -50.30128366834752995, -25.12097252146865145, 2.835025266119492571 ) ) ;
#11002=CARTESIAN_POINT ( 'NONE',  ( 12.41260344771940360, 16.11316662856288318, -1.500000000000002220 ) ) ;
#11003=ORIENTED_EDGE ( 'NONE', *, *, #33105, .T. ) ;
#11005=CARTESIAN_POINT ( 'NONE',  ( -43.52287095715007581, -23.47593901973090169, -1.443836447538997092 ) ) ;
#11006=CARTESIAN_POINT ( 'NONE',  ( -29.65134514979727953, -23.88619203586730677, 10.65365256123546978 ) ) ;
#11007=EDGE_CURVE ( 'NONE', #70027, #96494, #3707, .T. ) ;
#11008=CARTESIAN_POINT ( 'NONE',  ( -105.5507901751989692, -24.52300882791530512, 0.6510814631126371488 ) ) ;
#11011=CARTESIAN_POINT ( 'NONE',  ( -29.13856514152708499, -25.21531959831865066, 3.662308989302375029 ) ) ;
#11012=CARTESIAN_POINT ( 'NONE',  ( -49.35320922236618912, -25.31573769575033594, 4.652611179520380169 ) ) ;
#11013=ORIENTED_EDGE ( 'NONE', *, *, #80739, .F. ) ;
#11014=CARTESIAN_POINT ( 'NONE',  ( -0.3852054317258338245, -20.75737367715079174, 11.49999999999998934 ) ) ;
#11017=CARTESIAN_POINT ( 'NONE',  ( -125.5899157922687692, -24.40034930558991633, 0.3402023900116222244 ) ) ;
#11018=ORIENTED_EDGE ( 'NONE', *, *, #55162, .T. ) ;
#11019=B_SPLINE_SURFACE_WITH_KNOTS ( 'NONE', 3, 3, ( 
 ( #73202, #80807, #96523, #51355 ),
 ( #4185, #74678, #5668, #59467 ),
 ( #4685, #36127, #90408, #20883 ),
 ( #97024, #51857, #82790, #12274 ),
 ( #42271, #5172, #49875, #13270 ),
 ( #44246, #66608, #27523, #82295 ),
 ( #3690, #50365, #18894, #27019 ),
 ( #74192, #36618, #19888, #12773 ),
 ( #67587, #75174, #58973, #57985 ),
 ( #98504, #50862, #88422, #81301 ),
 ( #43743, #11786, #42756, #81799 ),
 ( #43252, #35633, #97518, #89912 ),
 ( #45732, #77663, #85286, #60478 ),
 ( #6662, #15774, #83286, #99499 ),
 ( #61967, #14264, #92393, #38109 ),
 ( #21375, #15270, #23371, #7667 ),
 ( #52847, #29995, #21871, #69065 ),
 ( #8171, #14766, #53852, #91394 ),
 ( #7160, #60969, #31000, #99990 ),
 ( #75663, #76656, #83786, #57 ),
 ( #6164, #45240, #91894, #84784 ),
 ( #30498, #22369, #92894, #61470 ),
 ( #37116, #22867, #76163, #54354 ),
 ( #68076, #37616, #53354, #46230 ),
 ( #39113, #70066, #38615, #99001 ) ),
 .UNSPECIFIED., .F., .F., .F.,
 ( 4, 3, 3, 3, 3, 3, 3, 3, 4 ),
 ( 4, 4 ),
 ( -9.884131503357096650E-16, 0.1249999999999991812, 0.1874999999999992784, 0.2499999999999993616, 0.4999999999999997224, 0.7500000000000001110, 0.8125000000000002220, 0.8750000000000002220, 1.000000000000000444 ),
 ( 0.000000000000000000, 1.000000000000000000 ),
 .UNSPECIFIED. ) ;
#11022=ORIENTED_EDGE ( 'NONE', *, *, #42355, .T. ) ;
#11023=VERTEX_POINT ( 'NONE', #90054 ) ;
#11024=B_SPLINE_CURVE_WITH_KNOTS ( 'NONE', 3,
 ( #64780, #21545, #44914, #12939, #20063, #4357, #59643, #60642 ),
 .UNSPECIFIED., .F., .F.,
 ( 4, 2, 2, 4 ),
 ( 0.000000000000000000, 0.002001079623178227563, 0.003001619434767338959, 0.004002159246356450789 ),
 .UNSPECIFIED. ) ;
#11025=CARTESIAN_POINT ( 'NONE',  ( -78.62287095715005592, -24.34917612406838217, 0.1852690917426633999 ) ) ;
#11027=CARTESIAN_POINT ( 'NONE',  ( -70.82359880940848029, -25.24515063934281400, 5.413474252732282110 ) ) ;
#11028=CARTESIAN_POINT ( 'NONE',  ( 6.148021820315829444, -21.18842874637755358, 11.49999999999999645 ) ) ;
#11031=CARTESIAN_POINT ( 'NONE',  ( -101.6228709571500701, -23.47596703998600631, 11.44779298504227683 ) ) ;
#11032=CARTESIAN_POINT ( 'NONE',  ( -15.94491270116497184, -16.04792668696150315, -1.500000000000002220 ) ) ;
#11035=EDGE_LOOP ( 'NONE', ( #72039, #94090, #55209, #65559 ) ) ;
#11036=ORIENTED_EDGE ( 'NONE', *, *, #22488, .T. ) ;
#11037=PLANE ( 'NONE',  #100045 ) ;
#11042=EDGE_LOOP ( 'NONE', ( #12826, #44946, #32367, #16472 ) ) ;
#11043=CARTESIAN_POINT ( 'NONE',  ( -6.524719417830534773, 20.15472526627327454, -1.500000000000002220 ) ) ;
#11044=CARTESIAN_POINT ( 'NONE',  ( -78.95422500253870624, -25.27791675628532531, 6.195240761392555306 ) ) ;
#11046=CARTESIAN_POINT ( 'NONE',  ( -125.6228709571500843, -24.51163499207175533, 0.6490370598554157100 ) ) ;
#11047=CARTESIAN_POINT ( 'NONE',  ( -39.58953762381673158, -23.47593901973091235, -1.443836447539011525 ) ) ;
#11048=CARTESIAN_POINT ( 'NONE',  ( 22.14152233036116257, 1.636640089565777334, -1.500000000000002220 ) ) ;
#11049=CARTESIAN_POINT ( 'NONE',  ( -49.25033725972690490, -25.13941398251548875, 7.108518452791937392 ) ) ;
#11053=EDGE_CURVE ( 'NONE', #81664, #90864, #2448, .T. ) ;
#11056=CARTESIAN_POINT ( 'NONE',  ( 4.731349760756693890, 18.90081699332259646, -1.500000000000002220 ) ) ;
#11058=CARTESIAN_POINT ( 'NONE',  ( -20.52298544035203776, 6.160189734329080125, 11.49999999999998934 ) ) ;
#11060=DIRECTION ( 'NONE',  ( -3.773278334453079030E-23, 0.9999999999976377785, 2.173523156925979128E-06 ) ) ;
#11061=CARTESIAN_POINT ( 'NONE',  ( -77.51696571866160923, -23.73766607897670156, -1.055555164236459564 ) ) ;
#11062=CARTESIAN_POINT ( 'NONE',  ( -9.230423729802735622, -20.81519635545753033, -1.500000000000002220 ) ) ;
#11064=CARTESIAN_POINT ( 'NONE',  ( -102.6362846996450173, -23.48783264082478439, -1.443836473390064601 ) ) ;
#11066=CARTESIAN_POINT ( 'NONE',  ( 14.98761344906185577, -13.09354923471379983, 11.49999999999999645 ) ) ;
#11067=DIRECTION ( 'NONE',  ( 3.773278334444166432E-23, -1.000000000000000000, 0.000000000000000000 ) ) ;
#11068=CARTESIAN_POINT ( 'NONE',  ( -89.23534077628077910, -25.27880950044346164, 5.947789066509455935 ) ) ;
#11073=CARTESIAN_POINT ( 'NONE',  ( -37.52287095715006870, -29.50248528299804818, 1.056150453629031594 ) ) ;
#11074=CARTESIAN_POINT ( 'NONE',  ( 16.98214085172422827, 13.50221961261776293, -1.500000000000002220 ) ) ;
#11075=CARTESIAN_POINT ( 'NONE',  ( -93.55620429048339304, -24.65952944569304606, 1.056160979905701902 ) ) ;
#11076=CARTESIAN_POINT ( 'NONE',  ( 2.510080532074158377, -19.39449211012750496, -1.500000000000002220 ) ) ;
#11078=ORIENTED_EDGE ( 'NONE', *, *, #5798, .T. ) ;
#11080=CARTESIAN_POINT ( 'NONE',  ( -69.86226385320381382, -29.50248914370730091, 2.832395270851967073 ) ) ;
#11081=CARTESIAN_POINT ( 'NONE',  ( 17.75789855128238770, 10.12834119215567164, 11.49999999999999645 ) ) ;
#11082=CARTESIAN_POINT ( 'NONE',  ( -85.55620429048340725, -23.47593901973091235, -1.443836447539002865 ) ) ;
#11083=ADVANCED_FACE ( 'NONE', ( #61112 ), #15911, .F. ) ;
#11084=FACE_OUTER_BOUND ( 'NONE', #49818, .T. ) ;
#11085=ORIENTED_EDGE ( 'NONE', *, *, #78638, .T. ) ;
#11086=PLANE ( 'NONE',  #99367 ) ;
#11087=CARTESIAN_POINT ( 'NONE',  ( -84.62287095715005592, -29.50250243563736774, 8.947779886222141599 ) ) ;
#11089=EDGE_CURVE ( 'NONE', #53102, #85507, #8309, .T. ) ;
#11091=ORIENTED_EDGE ( 'NONE', *, *, #40629, .F. ) ;
#11092=CARTESIAN_POINT ( 'NONE',  ( -42.58953762381671737, -24.65952944569304250, 1.056160979905689024 ) ) ;
#11094=CARTESIAN_POINT ( 'NONE',  ( 13.56796309060646166, -18.52494293750034871, 11.49999999999999645 ) ) ;
#11095=CARTESIAN_POINT ( 'NONE',  ( 16.48639501038195121, -15.69157857782056276, 11.49999999999998934 ) ) ;
#11096=CARTESIAN_POINT ( 'NONE',  ( -110.5518226189701494, -24.52399227489124556, 9.353111116836533512 ) ) ;
#11097=CARTESIAN_POINT ( 'NONE',  ( -75.62287095715007013, -24.15516710230293995, 10.28746687063726384 ) ) ;
#11099=CARTESIAN_POINT ( 'NONE',  ( -54.52287095715005449, -24.34917612406836795, 0.1852690917426491890 ) ) ;
#11100=CARTESIAN_POINT ( 'NONE',  ( -86.62287095715001328, -23.47596703998600631, 11.44779298504227683 ) ) ;
#11101=CARTESIAN_POINT ( 'NONE',  ( -4.983756199382824548, -21.29032736245130053, 11.49999999999998934 ) ) ;
#11102=CARTESIAN_POINT ( 'NONE',  ( -69.49771156051228616, -24.51419770103157347, 9.386484678747178734 ) ) ;
#11103=CARTESIAN_POINT ( 'NONE',  ( -26.11680270647584479, -24.94521091305072957, 4.366544573346394564 ) ) ;
#11104=CARTESIAN_POINT ( 'NONE',  ( -28.52287095715005805, -24.48836230353387222, 1.056161703005638719 ) ) ;
#11105=CARTESIAN_POINT ( 'NONE',  ( -47.92287095715006018, -23.47593901973090169, -1.443836447538997980 ) ) ;
#11108=CARTESIAN_POINT ( 'NONE',  ( -13.80512455850298714, -15.04058748057734896, 11.49999999999998934 ) ) ;
#11109=ORIENTED_EDGE ( 'NONE', *, *, #15364, .T. ) ;
#11110=VERTEX_POINT ( 'NONE', #92042 ) ;
#11112=CARTESIAN_POINT ( 'NONE',  ( 14.87233727408824713, -17.56007624320114857, 11.49999999999998934 ) ) ;
#11114=CARTESIAN_POINT ( 'NONE',  ( 17.97931717627152182, 9.192180251422895410, -1.500000000000002220 ) ) ;
#11117=CARTESIAN_POINT ( 'NONE',  ( -48.52287095715006870, -23.73934037231757088, 11.05740245334328620 ) ) ;
#11118=CARTESIAN_POINT ( 'NONE',  ( -77.62287095715005592, -29.50248528299804818, 1.056150453629038477 ) ) ;
#11119=CARTESIAN_POINT ( 'NONE',  ( -53.52206042989558199, -23.48786465467240703, 11.44779295918255002 ) ) ;
#11121=CARTESIAN_POINT ( 'NONE',  ( -15.06583839362908961, -15.15408912208086534, 11.49999999999999645 ) ) ;
#11122=ORIENTED_EDGE ( 'NONE', *, *, #21262, .T. ) ;
#11124=ORIENTED_EDGE ( 'NONE', *, *, #94048, .T. ) ;
#11125=CARTESIAN_POINT ( 'NONE',  ( 21.15429367616652101, -6.912965584596229895, -1.500000000000002220 ) ) ;
#11126=CARTESIAN_POINT ( 'NONE',  ( -20.51892249978613236, 2.527598752449112585, 11.49999999999998934 ) ) ;
#11127=B_SPLINE_CURVE_WITH_KNOTS ( 'NONE', 3,
 ( #69204, #39247, #78302, #92531, #45386, #85931 ),
 .UNSPECIFIED., .F., .F.,
 ( 4, 2, 4 ),
 ( 6.391158118964603462E-06, 0.001387004593080780291, 0.002767618028042595924 ),
 .UNSPECIFIED. ) ;
#11128=B_SPLINE_CURVE_WITH_KNOTS ( 'NONE', 3,
 ( #99867, #55238, #24755, #53730 ),
 .UNSPECIFIED., .F., .F.,
 ( 4, 4 ),
 ( 0.000000000000000000, 1.000000000000000000 ),
 .UNSPECIFIED. ) ;
#11129=ORIENTED_EDGE ( 'NONE', *, *, #25739, .T. ) ;
#11132=DIRECTION ( 'NONE',  ( -3.773278334453079030E-23, 0.9999999999976377785, 2.173523156925979128E-06 ) ) ;
#11134=CARTESIAN_POINT ( 'NONE',  ( -129.5228709571500758, -24.33832256527049154, 0.1851278514138698372 ) ) ;
#11135=ORIENTED_EDGE ( 'NONE', *, *, #81727, .T. ) ;
#11137=CARTESIAN_POINT ( 'NONE',  ( -8.544475976622297964, 19.10969517993760292, -1.500000000000002220 ) ) ;
#11138=CARTESIAN_POINT ( 'NONE',  ( -6.542779104410481494, 20.88585256366161502, 11.49999999999999645 ) ) ;
#11139=CARTESIAN_POINT ( 'NONE',  ( -73.62362711126294812, -24.66019654487200441, 8.947790411086119278 ) ) ;
#11140=CARTESIAN_POINT ( 'NONE',  ( -5.125883829288005344, 21.89707322345674712, 11.49999999999998934 ) ) ;
#11141=CARTESIAN_POINT ( 'NONE',  ( 11.32296221242833667, -17.63459971646239310, -1.500000000000002220 ) ) ;
#11142=LINE ( 'NONE', #42115, #40047 ) ;
#11144=CARTESIAN_POINT ( 'NONE',  ( -82.62287095715005592, -23.48786465467241413, 11.44779295918254647 ) ) ;
#11145=ORIENTED_EDGE ( 'NONE', *, *, #14850, .F. ) ;
#11149=VERTEX_POINT ( 'NONE', #31638 ) ;
#11151=CARTESIAN_POINT ( 'NONE',  ( 4.431377227695222132, -20.94745169971119481, -1.500000000000002220 ) ) ;
#11152=ORIENTED_EDGE ( 'NONE', *, *, #17456, .T. ) ;
#11155=CARTESIAN_POINT ( 'NONE',  ( 20.24497096899912307, 5.935080660949433096, -1.500000000000002220 ) ) ;
#11156=CARTESIAN_POINT ( 'NONE',  ( -30.43335359600822798, -24.47651708652394831, 9.440108529385041081 ) ) ;
#11159=CARTESIAN_POINT ( 'NONE',  ( -50.53932727748372145, -24.52399227489126687, 9.353111116836522854 ) ) ;
#11160=LINE ( 'NONE', #87792, #26462 ) ;
#11161=CARTESIAN_POINT ( 'NONE',  ( -129.6235275842055614, -24.51419770103158058, 9.386484678747178734 ) ) ;
#11162=CARTESIAN_POINT ( 'NONE',  ( 15.63414672909509839, 15.54323407889855879, -1.500000000000002220 ) ) ;
#11163=EDGE_LOOP ( 'NONE', ( #21112, #2245, #61927, #34709 ) ) ;
#11164=CARTESIAN_POINT ( 'NONE',  ( -65.63884284507189193, -24.40133493613049964, 9.663955038902800609 ) ) ;
#11165=B_SPLINE_CURVE_WITH_KNOTS ( 'NONE', 3,
 ( #3996, #34937, #27822, #11591 ),
 .UNSPECIFIED., .F., .F.,
 ( 4, 4 ),
 ( 0.2199429803762241731, 0.2289494116483397346 ),
 .UNSPECIFIED. ) ;
#11167=CARTESIAN_POINT ( 'NONE',  ( -63.62287095715004881, -23.47593901973091235, -1.443836447539007972 ) ) ;
#11168=ADVANCED_FACE ( 'NONE', ( #196 ), #61150, .T. ) ;
#11170=EDGE_CURVE ( 'NONE', #45447, #34154, #8553, .T. ) ;
#11171=CARTESIAN_POINT ( 'NONE',  ( -26.96874452920905085, -24.58296376597837707, 8.290116722409051064 ) ) ;
#11173=ADVANCED_FACE ( 'NONE', ( #83256 ), #89877, .T. ) ;
#11176=CARTESIAN_POINT ( 'NONE',  ( 21.32124590881793225, -1.116183810207903804, -1.500000000000002220 ) ) ;
#11177=CARTESIAN_POINT ( 'NONE',  ( -92.52287095715006160, -23.47596703998600631, 11.44779298504228393 ) ) ;
#11178=CARTESIAN_POINT ( 'NONE',  ( -34.62287095715005592, -23.47593901973091235, -1.443836447539013301 ) ) ;
#11179=DIRECTION ( 'NONE',  ( 1.000000000000000000, 3.773278334444166432E-23, 8.201307841325785021E-29 ) ) ;
#11181=CARTESIAN_POINT ( 'NONE',  ( 10.27952223434480494, 20.12118371629609470, -1.500000000000002220 ) ) ;
#11185=CARTESIAN_POINT ( 'NONE',  ( -79.60526328347016545, -23.48783264082476308, -1.443836473390096575 ) ) ;
#11186=CARTESIAN_POINT ( 'NONE',  ( 15.11087362536062173, -12.71848776332401521, 11.49999999999999645 ) ) ;
#11188=CARTESIAN_POINT ( 'NONE',  ( -96.58953762381672448, -23.47593901973091235, -1.443836447539001089 ) ) ;
#11189=EDGE_CURVE ( 'NONE', #50453, #40343, #71465, .T. ) ;
#11191=CARTESIAN_POINT ( 'NONE',  ( -117.5895376238167103, -24.65952944569305316, 1.056160979905702790 ) ) ;
#11193=CARTESIAN_POINT ( 'NONE',  ( -100.5528973737291238, -25.12268565405453913, 7.099974650722071345 ) ) ;
#11194=CARTESIAN_POINT ( 'NONE',  ( 17.58597629297885589, -12.55149374826878272, 11.49999999999998934 ) ) ;
#11195=CARTESIAN_POINT ( 'NONE',  ( -71.62287095715005592, -23.47596703998600631, 11.44779298504227683 ) ) ;
#11196=CARTESIAN_POINT ( 'NONE',  ( -66.52287095715010423, -24.51387760970724727, 9.387446482453405849 ) ) ;
#11198=CARTESIAN_POINT ( 'NONE',  ( -118.5562042904833930, -24.64965694238575367, 8.947790433994192938 ) ) ;
#11199=CARTESIAN_POINT ( 'NONE',  ( -16.30015253881794379, -11.17962500214296639, -1.500000000000002220 ) ) ;
#11200=ORIENTED_EDGE ( 'NONE', *, *, #29130, .T. ) ;
#11201=CARTESIAN_POINT ( 'NONE',  ( -15.58492919356500650, -12.95507736684500699, 11.49999999999999645 ) ) ;
#11204=EDGE_CURVE ( 'NONE', #83628, #45754, #22339, .T. ) ;
#11205=ORIENTED_EDGE ( 'NONE', *, *, #66550, .F. ) ;
#11206=CARTESIAN_POINT ( 'NONE',  ( -40.58953762381673158, -23.47593901973091235, -1.443836447539011525 ) ) ;
#11209=CARTESIAN_POINT ( 'NONE',  ( -82.62287095715005592, -23.94994826722566117, -0.6494450866342736939 ) ) ;
#11210=CARTESIAN_POINT ( 'NONE',  ( -39.62287095715008434, -24.51283580621364777, 0.6167428607019764808 ) ) ;
#11211=CARTESIAN_POINT ( 'NONE',  ( -96.52287095715006160, -24.51283580621364422, 0.6167428607019779241 ) ) ;
#11212=CARTESIAN_POINT ( 'NONE',  ( 19.28819943863484454, -5.468471092112969778, -1.500000000000002220 ) ) ;
#11213=EDGE_CURVE ( 'NONE', #98513, #63968, #66623, .T. ) ;
#11215=ORIENTED_EDGE ( 'NONE', *, *, #82072, .F. ) ;
#11216=EDGE_CURVE ( 'NONE', #16993, #6143, #31543, .T. ) ;
#11217=EDGE_CURVE ( 'NONE', #14515, #54685, #94446, .T. ) ;
#11219=CARTESIAN_POINT ( 'NONE',  ( -33.62287095715007013, -24.51283580621364422, 0.6167428607019749265 ) ) ;
#11220=CARTESIAN_POINT ( 'NONE',  ( -63.58953762381672448, -24.64965694238575011, 8.947790433994200043 ) ) ;
#11222=CARTESIAN_POINT ( 'NONE',  ( -103.5228709571501184, -24.51283580621365843, 0.6167428607019787012 ) ) ;
#11224=CARTESIAN_POINT ( 'NONE',  ( -51.54161239871793043, -25.23256535379771037, 6.480020017899467355 ) ) ;
#11225=VERTEX_POINT ( 'NONE', #53504 ) ;
#11227=CARTESIAN_POINT ( 'NONE',  ( -19.79944955726156763, -4.570829099900970860, -1.500000000000002220 ) ) ;
#11229=CARTESIAN_POINT ( 'NONE',  ( -4.681240387505234857, -22.43558246840685300, -1.500000000000002220 ) ) ;
#11231=CARTESIAN_POINT ( 'NONE',  ( -127.6240570307130611, -24.15620529776628800, 10.23563542870658871 ) ) ;
#11235=VECTOR ( 'NONE', #45944, 1000.000000000000227 ) ;
#11236=CARTESIAN_POINT ( 'NONE',  ( -30.47287095715006799, -24.05195403655357111, -0.4597278507670095604 ) ) ;
#11237=CARTESIAN_POINT ( 'NONE',  ( -15.86343167427570577, 14.10970434637795634, 11.49999999999999645 ) ) ;
#11239=CARTESIAN_POINT ( 'NONE',  ( 22.15222936869060177, 0.07132910108538677296, 11.49999999999998934 ) ) ;
#11240=CARTESIAN_POINT ( 'NONE',  ( 10.54205562766345672, -17.70522803435136083, -1.500000000000002220 ) ) ;
#11242=ORIENTED_EDGE ( 'NONE', *, *, #13810, .F. ) ;
#11243=CARTESIAN_POINT ( 'NONE',  ( -111.5228709571500190, -23.48783264082477018, -1.443836473390084585 ) ) ;
#11251=CARTESIAN_POINT ( 'NONE',  ( -61.24303308397303880, -29.50249942614373921, 7.563164501610022405 ) ) ;
#11253=CARTESIAN_POINT ( 'NONE',  ( -9.423985339279758122, -18.44656043379632848, -1.500000000000002220 ) ) ;
#11254=CARTESIAN_POINT ( 'NONE',  ( 19.97611268498323511, -8.487024919450899318, 11.49999999999999645 ) ) ;
#11258=CARTESIAN_POINT ( 'NONE',  ( 11.21425909587273928, 19.38466839394011387, -1.500000000000002220 ) ) ;
#11259=CARTESIAN_POINT ( 'NONE',  ( -124.5562042904833930, -23.48783264082478794, -1.443836473390058384 ) ) ;
#11260=CARTESIAN_POINT ( 'NONE',  ( -61.55620429048339304, -24.64965694238573946, 8.947790433994205372 ) ) ;
#11265=ORIENTED_EDGE ( 'NONE', *, *, #32838, .T. ) ;
#11266=CARTESIAN_POINT ( 'NONE',  ( -112.5228709571500616, -24.66019654487200441, 8.947790411086108620 ) ) ;
#11269=CARTESIAN_POINT ( 'NONE',  ( -15.86343167427570577, 14.10970434637795634, -1.500000000000002220 ) ) ;
#11273=CARTESIAN_POINT ( 'NONE',  ( 3.337383349182757364, -21.60657791699550856, -1.500000000000002220 ) ) ;
#11274=CARTESIAN_POINT ( 'NONE',  ( -103.6332108804325571, -23.73791477778911840, 11.05961554403170410 ) ) ;
#11277=CARTESIAN_POINT ( 'NONE',  ( 19.92038474643397805, 8.973206291307779026, -1.500000000000002220 ) ) ;
#11279=ORIENTED_EDGE ( 'NONE', *, *, #27799, .F. ) ;
#11281=LINE ( 'NONE', #43246, #73489 ) ;
#11282=ADVANCED_FACE ( 'NONE', ( #40263 ), #36802, .T. ) ;
#11286=CARTESIAN_POINT ( 'NONE',  ( -30.63563248976338826, -23.78419283595092537, 10.96997220532171369 ) ) ;
#11289=EDGE_CURVE ( 'NONE', #90864, #65243, #95044, .T. ) ;
#11291=CARTESIAN_POINT ( 'NONE',  ( -12.29646723538143505, -17.35194501319736560, 11.49999999999998934 ) ) ;
#11292=DIRECTION ( 'NONE',  ( 0.000000000000000000, 0.9999999999976377785, 2.173523156925979975E-06 ) ) ;
#11294=VECTOR ( 'NONE', #27725, 1000.000000000000114 ) ;
#11295=PLANE ( 'NONE',  #60002 ) ;
#11296=CARTESIAN_POINT ( 'NONE',  ( -108.6228709571500417, -23.47596703998600631, 11.44779298504227860 ) ) ;
#11297=CARTESIAN_POINT ( 'NONE',  ( -13.55963120218723361, -13.89248740512243430, 11.49999999999998934 ) ) ;
#11299=ORIENTED_EDGE ( 'NONE', *, *, #74509, .T. ) ;
#11300=CARTESIAN_POINT ( 'NONE',  ( 19.52168601723349894, 1.684101417132040979, 11.49999999999999645 ) ) ;
#11304=ADVANCED_FACE ( 'NONE', ( #48380 ), #75671, .T. ) ;
#11305=VERTEX_POINT ( 'NONE', #49392 ) ;
#11307=DIRECTION ( 'NONE',  ( 0.000000000000000000, 2.173523156925980399E-06, -0.9999999999976378895 ) ) ;
#11310=DIRECTION ( 'NONE',  ( -3.773278334453080206E-23, 0.9999999999976377785, 2.173523156925979975E-06 ) ) ;
#11311=CARTESIAN_POINT ( 'NONE',  ( 15.21843288076463629, 12.49332292251147614, -1.500000000000002220 ) ) ;
#11314=VERTEX_POINT ( 'NONE', #65125 ) ;
#11316=CARTESIAN_POINT ( 'NONE',  ( -78.52287095715006160, -24.65952944569304606, 1.056160979905698794 ) ) ;
#11317=DIRECTION ( 'NONE',  ( -3.773278334444167608E-23, 1.000000000000000000, 0.000000000000000000 ) ) ;
#11318=EDGE_CURVE ( 'NONE', #75985, #64522, #80827, .T. ) ;
#11319=VECTOR ( 'NONE', #36751, 1000.000000000000114 ) ;
#11321=VERTEX_POINT ( 'NONE', #42291 ) ;
#11324=FACE_OUTER_BOUND ( 'NONE', #38483, .T. ) ;
#11325=CARTESIAN_POINT ( 'NONE',  ( -29.52287095715006515, -23.64153651536914680, 11.05761042422066787 ) ) ;
#11326=CARTESIAN_POINT ( 'NONE',  ( -78.92430620016367016, -25.33009845126374415, 4.495758016894969344 ) ) ;
#11327=DIRECTION ( 'NONE',  ( 3.773278334444167608E-23, -1.000000000000000000, 0.000000000000000000 ) ) ;
#11329=CARTESIAN_POINT ( 'NONE',  ( -12.66726347749767179, -15.43046242340049545, 11.49999999999998934 ) ) ;
#11331=CARTESIAN_POINT ( 'NONE',  ( 17.57725459251073019, -9.329341740261039462, -1.500000000000002220 ) ) ;
#11333=CARTESIAN_POINT ( 'NONE',  ( -122.5228709571500474, -23.95044443724993144, 10.65354141964648882 ) ) ;
#11334=EDGE_CURVE ( 'NONE', #99120, #10131, #42357, .T. ) ;
#11335=CARTESIAN_POINT ( 'NONE',  ( -29.52287095715006160, -23.40102634903646717, 11.44779303447556629 ) ) ;
#11336=FACE_OUTER_BOUND ( 'NONE', #45222, .T. ) ;
#11337=CARTESIAN_POINT ( 'NONE',  ( 19.92439739378097840, -5.974006126113303949, 11.49999999999999645 ) ) ;
#11340=EDGE_CURVE ( 'NONE', #64814, #100208, #7093, .T. ) ;
#11342=CARTESIAN_POINT ( 'NONE',  ( -18.69919181139871966, -13.08804974640095686, 11.49999999999999645 ) ) ;
#11344=CARTESIAN_POINT ( 'NONE',  ( -43.52287095715006160, -24.64898659630528854, 1.056161002820819261 ) ) ;
#11345=FACE_OUTER_BOUND ( 'NONE', #13829, .T. ) ;
#11347=CARTESIAN_POINT ( 'NONE',  ( 12.36038202409810438, -16.04522380935875248, -1.500000000000002220 ) ) ;
#11351=B_SPLINE_CURVE_WITH_KNOTS ( 'NONE', 3,
 ( #33346, #65341, #26744, #87140, #25744, #17629 ),
 .UNSPECIFIED., .F., .F.,
 ( 4, 2, 4 ),
 ( 0.000000000000000000, 0.001380764517854764966, 0.002761529035709529931 ),
 .UNSPECIFIED. ) ;
#11352=CARTESIAN_POINT ( 'NONE',  ( -100.6228709571500701, -23.85196035786901447, -0.8779234886474918120 ) ) ;
#11353=B_SPLINE_CURVE_WITH_KNOTS ( 'NONE', 3,
 ( #1093, #93930, #22893, #32036, #53882, #69605 ),
 .UNSPECIFIED., .F., .F.,
 ( 4, 2, 4 ),
 ( 1.570755371634395932E-05, 0.001396183895866091006, 0.002776660238015837747 ),
 .UNSPECIFIED. ) ;
#11354=ORIENTED_EDGE ( 'NONE', *, *, #32774, .T. ) ;
#11355=CARTESIAN_POINT ( 'NONE',  ( -79.35175030129791196, -25.28818030286010909, 5.821563397865827660 ) ) ;
#11357=CARTESIAN_POINT ( 'NONE',  ( -7.287290609967129740, 18.71191762695291771, -1.500000000000002220 ) ) ;
#11358=CARTESIAN_POINT ( 'NONE',  ( 11.68726034403320746, 17.49698133428071145, 11.49999999999999645 ) ) ;
#11360=CARTESIAN_POINT ( 'NONE',  ( -93.52287095715006160, -24.35013146730204525, 9.818937971375095941 ) ) ;
#11361=CARTESIAN_POINT ( 'NONE',  ( 8.687672273659204691, 20.25853876245846408, 11.49999999999998934 ) ) ;
#11362=AXIS2_PLACEMENT_3D ( 'NONE', #60558, #76734, #62543 ) ;
#11366=CARTESIAN_POINT ( 'NONE',  ( -90.70649462243461869, -25.27880950044346164, 5.947789066509452383 ) ) ;
#11367=CARTESIAN_POINT ( 'NONE',  ( -86.55620429048336462, -24.65952944569304606, 1.056160979905700348 ) ) ;
#11368=VERTEX_POINT ( 'NONE', #44264 ) ;
#11369=ORIENTED_EDGE ( 'NONE', *, *, #27890, .T. ) ;
#11372=CARTESIAN_POINT ( 'NONE',  ( -108.6228709571500559, -29.50250786944525672, 11.44777988621622988 ) ) ;
#11373=CARTESIAN_POINT ( 'NONE',  ( -17.34406541665444124, 10.97931167347951842, -1.500000000000002220 ) ) ;
#11374=ORIENTED_EDGE ( 'NONE', *, *, #88853, .F. ) ;
#11378=CARTESIAN_POINT ( 'NONE',  ( 2.183928509170398602, -22.20744181112294413, -1.500000000000002220 ) ) ;
#11380=CARTESIAN_POINT ( 'NONE',  ( -124.6228709571500417, -24.65952944569304606, 1.056160979905705011 ) ) ;
#11381=VERTEX_POINT ( 'NONE', #75194 ) ;
#11382=CARTESIAN_POINT ( 'NONE',  ( -31.66446019296014569, -24.86181185134534388, 1.747789972853592833 ) ) ;
#11383=LINE ( 'NONE', #43344, #23127 ) ;
#11385=CARTESIAN_POINT ( 'NONE',  ( -20.60679684081203789, -3.318877370925724879, -1.500000000000002220 ) ) ;
#11387=CARTESIAN_POINT ( 'NONE',  ( -39.11412362507491025, -25.24269817073092170, 3.764647656015266186 ) ) ;
#11389=ORIENTED_EDGE ( 'NONE', *, *, #21138, .F. ) ;
#11391=CARTESIAN_POINT ( 'NONE',  ( -33.52287095715006160, -23.47593901973090169, -1.443836447538997314 ) ) ;
#11392=CARTESIAN_POINT ( 'NONE',  ( -3.607955376466517095, 20.77440192976073519, -1.500000000000002220 ) ) ;
#11395=ORIENTED_EDGE ( 'NONE', *, *, #76437, .F. ) ;
#11397=CARTESIAN_POINT ( 'NONE',  ( -48.91478977402367434, -25.27868427054752587, 5.813191968676703958 ) ) ;
#11398=ADVANCED_FACE ( 'NONE', ( #67605 ), #23276, .T. ) ;
#11399=CARTESIAN_POINT ( 'NONE',  ( -120.5534771641331133, -24.63419186844610920, 9.035850630976920428 ) ) ;
#11400=EDGE_CURVE ( 'NONE', #86526, #21106, #91920, .T. ) ;
#11401=CARTESIAN_POINT ( 'NONE',  ( -76.58462478488942793, -24.51419770103157347, 9.386484678747176957 ) ) ;
#11403=CARTESIAN_POINT ( 'NONE',  ( -11.49108604648090548, 18.38894055434275643, -1.500000000000002220 ) ) ;
#11404=CARTESIAN_POINT ( 'NONE',  ( -80.48900664166535535, -25.12224392042292820, 7.101635560657246771 ) ) ;
#11405=CARTESIAN_POINT ( 'NONE',  ( -13.70410651198969809, -17.55484038775568933, 11.49999999999999645 ) ) ;
#11406=VERTEX_POINT ( 'NONE', #12791 ) ;
#11407=CARTESIAN_POINT ( 'NONE',  ( -50.41832839342763606, -25.31441722420615648, 5.198500813728550440 ) ) ;
#11408=CARTESIAN_POINT ( 'NONE',  ( -92.55620429048336462, -23.47596703998600631, 11.44779298504227683 ) ) ;
#11409=LINE ( 'NONE', #2812, #24576 ) ;
#11410=ORIENTED_EDGE ( 'NONE', *, *, #21702, .T. ) ;
#11411=EDGE_CURVE ( 'NONE', #98033, #84710, #100390, .T. ) ;
#11417=CARTESIAN_POINT ( 'NONE',  ( -88.62287095715004170, -23.72773821059535848, 11.05748984161097503 ) ) ;
#11418=CARTESIAN_POINT ( 'NONE',  ( -35.52287095715009713, -24.14321612903113845, -0.2833117244521470290 ) ) ;
#11420=ORIENTED_EDGE ( 'NONE', *, *, #21846, .T. ) ;
#11421=CARTESIAN_POINT ( 'NONE',  ( -130.5728709571500872, -24.82780549326299280, 8.726980033514458057 ) ) ;
#11422=CARTESIAN_POINT ( 'NONE',  ( 21.16529133594374557, -7.503415950508986576, -1.500000000000002220 ) ) ;
#11424=CARTESIAN_POINT ( 'NONE',  ( -98.89667099290487329, -25.25590005895643486, 6.210304623333523288 ) ) ;
#11425=CARTESIAN_POINT ( 'NONE',  ( -101.5124320122265260, -24.35071581493543746, 9.817618358456027039 ) ) ;
#11428=CARTESIAN_POINT ( 'NONE',  ( -63.90635909705261497, -25.30558673197061026, 5.002395802403323266 ) ) ;
#11429=CARTESIAN_POINT ( 'NONE',  ( -3.586273028688536257, -19.27814873881845514, 11.49999999999998934 ) ) ;
#11431=VERTEX_POINT ( 'NONE', #81820 ) ;
#11432=CARTESIAN_POINT ( 'NONE',  ( 7.253797376210795456, 20.28272692992397808, -1.500000000000002220 ) ) ;
#11433=CARTESIAN_POINT ( 'NONE',  ( -128.5895405319625695, -24.51314013834317862, 0.6176544820404316072 ) ) ;
#11434=CARTESIAN_POINT ( 'NONE',  ( -114.5228709571500900, -24.33832256527049864, 0.1851278514138636755 ) ) ;
#11435=CARTESIAN_POINT ( 'NONE',  ( -101.0641960954074534, -25.14446816578130850, 2.968297954937114458 ) ) ;
#11437=CARTESIAN_POINT ( 'NONE',  ( -77.62287095715002749, -24.51387760970723662, 9.387446482453407626 ) ) ;
#11438=CARTESIAN_POINT ( 'NONE',  ( -3.094460115123966570, -22.75893099265358188, -1.500000000000002220 ) ) ;
#11441=CARTESIAN_POINT ( 'NONE',  ( -53.49130680602832655, -24.51314013834315730, 0.6176544820404108460 ) ) ;
#11442=CARTESIAN_POINT ( 'NONE',  ( 18.99975792849237877, 6.539580213093530325, 11.49999999999999645 ) ) ;
#11444=CARTESIAN_POINT ( 'NONE',  ( -32.53164638043851653, -24.51419770103159834, 9.386484678747182286 ) ) ;
#11445=PLANE ( 'NONE',  #19811 ) ;
#11446=FACE_OUTER_BOUND ( 'NONE', #9413, .T. ) ;
#11448=CARTESIAN_POINT ( 'NONE',  ( -2.735935421901279696, -19.66989661884619522, -1.500000000000002220 ) ) ;
#11450=CARTESIAN_POINT ( 'NONE',  ( 19.16472379399037251, -4.548241762842377689, -1.500000000000002220 ) ) ;
#11452=CARTESIAN_POINT ( 'NONE',  ( -42.61653805103011905, -23.48783264082477373, -1.443836473390076147 ) ) ;
#11459=CARTESIAN_POINT ( 'NONE',  ( 18.80685554986811070, -8.408966509905500430, 11.49999999999999645 ) ) ;
#11460=EDGE_CURVE ( 'NONE', #22752, #21356, #43419, .T. ) ;
#11461=CARTESIAN_POINT ( 'NONE',  ( -42.62287095715007013, -23.73907113216990084, -1.053371485793237250 ) ) ;
#11462=CARTESIAN_POINT ( 'NONE',  ( 8.854694546379761277, 20.84150027139232364, 11.49999999999999645 ) ) ;
#11463=VERTEX_POINT ( 'NONE', #28036 ) ;
#11464=EDGE_CURVE ( 'NONE', #69290, #97480, #61560, .T. ) ;
#11465=CARTESIAN_POINT ( 'NONE',  ( -99.62287095715005592, -29.50248528299804818, 1.056150453629042030 ) ) ;
#11466=CARTESIAN_POINT ( 'NONE',  ( -50.80821443252320080, -25.31060262516012926, 4.652599235852771464 ) ) ;
#11467=CARTESIAN_POINT ( 'NONE',  ( -26.35953173686715800, -24.61459992720930501, 7.694642789483244094 ) ) ;
#11468=FACE_OUTER_BOUND ( 'NONE', #22052, .T. ) ;
#11470=ORIENTED_EDGE ( 'NONE', *, *, #9377, .T. ) ;
#11471=CARTESIAN_POINT ( 'NONE',  ( -99.77787996869076892, -25.14990886459445107, 6.942063247122693070 ) ) ;
#11472=CARTESIAN_POINT ( 'NONE',  ( -21.29394331855728240, -8.360804490491451801, -1.500000000000002220 ) ) ;
#11473=CARTESIAN_POINT ( 'NONE',  ( -110.4715243189340299, -25.18566208650414140, 3.299076066840834098 ) ) ;
#11475=CARTESIAN_POINT ( 'NONE',  ( -76.62287095715007013, -23.48786465467241058, 11.44779295918254469 ) ) ;
#11476=CARTESIAN_POINT ( 'NONE',  ( -15.53634343318938704, 16.32316209468629253, 11.49999999999999645 ) ) ;
#11477=ORIENTED_EDGE ( 'NONE', *, *, #78539, .F. ) ;
#11478=CARTESIAN_POINT ( 'NONE',  ( -89.81226385320383088, -25.13785473458314712, 7.104038777044550557 ) ) ;
#11479=CARTESIAN_POINT ( 'NONE',  ( -18.59763704738199408, -11.70098744416181979, 11.49999999999998934 ) ) ;
#11481=CARTESIAN_POINT ( 'NONE',  ( -29.17238308422418669, -24.79699977470989936, 6.041340515266470312 ) ) ;
#11483=DIRECTION ( 'NONE',  ( -3.773278334453079030E-23, 0.9999999999976377785, 2.173523156925979128E-06 ) ) ;
#11487=CARTESIAN_POINT ( 'NONE',  ( 20.06376955418885899, 4.186446014007643157, 11.49999999999998934 ) ) ;
#11488=ORIENTED_EDGE ( 'NONE', *, *, #95820, .F. ) ;
#11489=ORIENTED_EDGE ( 'NONE', *, *, #70993, .F. ) ;
#11490=ORIENTED_EDGE ( 'NONE', *, *, #97076, .F. ) ;
#11492=CARTESIAN_POINT ( 'NONE',  ( -3.594920434497504758, 22.80983129501555950, -1.500000000000002220 ) ) ;
#11493=CARTESIAN_POINT ( 'NONE',  ( -64.22287095715006444, -23.47596703998600631, 11.44779298504227683 ) ) ;
#11494=CARTESIAN_POINT ( 'NONE',  ( -8.236308187080631171, 18.58821751820538637, -1.500000000000002220 ) ) ;
#11497=CARTESIAN_POINT ( 'NONE',  ( -29.57134449316367864, -23.40477069770800966, 11.44779303447556806 ) ) ;
#11498=EDGE_CURVE ( 'NONE', #8268, #65583, #44670, .T. ) ;
#11499=CARTESIAN_POINT ( 'NONE',  ( -105.5884215510445046, -24.63355581998386157, 0.9682620441943899925 ) ) ;
#11500=CARTESIAN_POINT ( 'NONE',  ( -70.40598983096596442, -25.03149849373329872, 7.561209383477862644 ) ) ;
#11501=ORIENTED_EDGE ( 'NONE', *, *, #36459, .T. ) ;
#11502=CARTESIAN_POINT ( 'NONE',  ( -112.6228709571500701, -23.48786465467241769, 11.44779295918254114 ) ) ;
#11503=CARTESIAN_POINT ( 'NONE',  ( -86.55620429048337883, -23.48786465467241058, 11.44779295918254292 ) ) ;
#11505=CARTESIAN_POINT ( 'NONE',  ( -13.51810693421681719, -15.76408947421354156, -1.500000000000002220 ) ) ;
#11507=ORIENTED_EDGE ( 'NONE', *, *, #18065, .T. ) ;
#11509=EDGE_LOOP ( 'NONE', ( #66343, #55027, #6189, #94328 ) ) ;
#11510=CARTESIAN_POINT ( 'NONE',  ( -41.61685852264373864, -23.48786465467240347, 11.44779295918255180 ) ) ;
#11512=ORIENTED_EDGE ( 'NONE', *, *, #100, .T. ) ;
#11513=ORIENTED_EDGE ( 'NONE', *, *, #60898, .F. ) ;
#11517=CARTESIAN_POINT ( 'NONE',  ( -43.56067035728424486, -23.73791477778911130, 11.05961554403171121 ) ) ;
#11518=CARTESIAN_POINT ( 'NONE',  ( -4.445301477617020325, 21.63612927058290936, 11.49999999999999645 ) ) ;
#11519=ORIENTED_EDGE ( 'NONE', *, *, #16702, .F. ) ;
#11520=CARTESIAN_POINT ( 'NONE',  ( -103.5929782930063681, -23.96119346886881019, -0.6495511937832079141 ) ) ;
#11521=ADVANCED_FACE ( 'NONE', ( #69967 ), #18182, .T. ) ;
#11522=CARTESIAN_POINT ( 'NONE',  ( -20.05226876979747530, -10.47825485868949613, 11.49999999999998934 ) ) ;
#11524=DIRECTION ( 'NONE',  ( -3.773278334453079030E-23, 0.9999999999976377785, 2.173523156925979128E-06 ) ) ;
#11527=EDGE_CURVE ( 'NONE', #9990, #91541, #63384, .T. ) ;
#11528=ORIENTED_EDGE ( 'NONE', *, *, #2203, .F. ) ;
#11533=ORIENTED_EDGE ( 'NONE', *, *, #50356, .F. ) ;
#11534=CARTESIAN_POINT ( 'NONE',  ( -9.521469661382619520, 18.92286876745961166, -1.500000000000002220 ) ) ;
#11536=CARTESIAN_POINT ( 'NONE',  ( -39.55620429048340014, -23.47593901973091235, -1.443836447539011525 ) ) ;
#11537=CARTESIAN_POINT ( 'NONE',  ( 22.08996893241407378, 3.065900275835479860, -1.500000000000002220 ) ) ;
#11543=CARTESIAN_POINT ( 'NONE',  ( -36.60104952365126962, -23.96169478059712432, 10.65365249895718591 ) ) ;
#11545=CARTESIAN_POINT ( 'NONE',  ( 5.544562197198338538, -18.70016399976332977, -1.500000000000002220 ) ) ;
#11546=CARTESIAN_POINT ( 'NONE',  ( 14.05358622956002357, 16.19628355576825385, -1.500000000000002220 ) ) ;
#11550=CARTESIAN_POINT ( 'NONE',  ( -22.17926634000774655, 4.976981427743210951, -1.500000000000002220 ) ) ;
#11552=CARTESIAN_POINT ( 'NONE',  ( -98.54805141098935906, -24.51314013834315020, 0.6176544820404104019 ) ) ;
#11554=CARTESIAN_POINT ( 'NONE',  ( 5.901097582950029619, 19.04237314665466485, 11.49999999999999645 ) ) ;
#11555=DIRECTION ( 'NONE',  ( -0.000000000000000000, 2.173523156925979552E-06, -0.9999999999976378895 ) ) ;
#11557=DIRECTION ( 'NONE',  ( 3.773278334444166432E-23, -1.000000000000000000, 0.000000000000000000 ) ) ;
#11558=ORIENTED_EDGE ( 'NONE', *, *, #73559, .F. ) ;
#11561=CARTESIAN_POINT ( 'NONE',  ( -33.00279783456706895, -25.16370864782812689, 7.203858152271859439 ) ) ;
#11562=CARTESIAN_POINT ( 'NONE',  ( 19.61570337458852364, 9.273991169892711994, 11.49999999999998934 ) ) ;
#11563=CARTESIAN_POINT ( 'NONE',  ( -56.56717682641941991, -23.48786465467241058, 11.44779295918254647 ) ) ;
#11564=CARTESIAN_POINT ( 'NONE',  ( -17.64752530894654470, 8.349842952099315596, -1.500000000000002220 ) ) ;
#11566=ADVANCED_FACE ( 'NONE', ( #23787 ), #55764, .F. ) ;
#11568=CARTESIAN_POINT ( 'NONE',  ( -60.62287095715004881, -25.00182538069145011, 7.747789668545098429 ) ) ;
#11569=CARTESIAN_POINT ( 'NONE',  ( -20.44062828730913139, -1.133067592104922694, 11.49999999999999645 ) ) ;
#11573=CARTESIAN_POINT ( 'NONE',  ( -39.62287095715005592, -23.72773821059535493, 11.05748984161097503 ) ) ;
#11574=B_SPLINE_CURVE_WITH_KNOTS ( 'NONE', 3,
 ( #2841, #49513, #4332, #80447 ),
 .UNSPECIFIED., .F., .F.,
 ( 4, 4 ),
 ( 0.000000000000000000, 9.999999999998897304E-05 ),
 .UNSPECIFIED. ) ;
#11580=CARTESIAN_POINT ( 'NONE',  ( -49.28110964179429487, -25.25138858776646700, 6.053971624764486137 ) ) ;
#11581=CARTESIAN_POINT ( 'NONE',  ( -109.6292162128046499, -23.96119346886880663, -0.6495511937832053606 ) ) ;
#11582=VERTEX_POINT ( 'NONE', #86691 ) ;
#11583=CARTESIAN_POINT ( 'NONE',  ( -81.62287095715005592, -23.48783264082478794, -1.443836473390065711 ) ) ;
#11585=CARTESIAN_POINT ( 'NONE',  ( 22.09143763772896918, 6.410036269187016522, 11.49999999999999645 ) ) ;
#11586=CARTESIAN_POINT ( 'NONE',  ( -7.854035805165779927, 21.33931789143995417, -1.500000000000002220 ) ) ;
#11587=CARTESIAN_POINT ( 'NONE',  ( -110.5132562145541470, -24.63419186844610920, 9.035850630976920428 ) ) ;
#11588=DIRECTION ( 'NONE',  ( -3.773278334453079030E-23, 0.9999999999976377785, 2.173523156925979128E-06 ) ) ;
#11589=CARTESIAN_POINT ( 'NONE',  ( -90.52212989865935810, -23.48783264082477018, -1.443836473390091690 ) ) ;
#11591=CARTESIAN_POINT ( 'NONE',  ( -53.52287095715008292, -23.47593901973090169, -1.443836447538997092 ) ) ;
#11592=CARTESIAN_POINT ( 'NONE',  ( -89.52287095715006160, -24.65952944569304606, 1.056160979905700570 ) ) ;
#11593=CARTESIAN_POINT ( 'NONE',  ( -21.85961425739535358, 0.8689724601130633941, 11.49999999999998934 ) ) ;
#11595=CARTESIAN_POINT ( 'NONE',  ( -77.52287095715006160, -29.50250243563736774, 8.947779886222141599 ) ) ;
#11599=EDGE_LOOP ( 'NONE', ( #11135, #5137, #23571, #45095 ) ) ;
#11600=CARTESIAN_POINT ( 'NONE',  ( -4.163110563111144913, -19.98234244090558320, 11.49999999999998934 ) ) ;
#11601=VERTEX_POINT ( 'NONE', #2467 ) ;
#11602=ORIENTED_EDGE ( 'NONE', *, *, #70748, .T. ) ;
#11604=ORIENTED_EDGE ( 'NONE', *, *, #55396, .T. ) ;
#11605=CARTESIAN_POINT ( 'NONE',  ( 20.85440106035463970, 9.703512019146668166, 11.49999999999998934 ) ) ;
#11606=LINE ( 'NONE', #57316, #72966 ) ;
#11607=CARTESIAN_POINT ( 'NONE',  ( 1.109688723463823301, -20.12803150795971874, -1.500000000000002220 ) ) ;
#11609=PLANE ( 'NONE',  #49387 ) ;
#11611=CARTESIAN_POINT ( 'NONE',  ( -95.50802337316835633, -24.52300882791530512, 0.6510814631126408125 ) ) ;
#11612=CARTESIAN_POINT ( 'NONE',  ( -123.5228709571500474, -23.47593901973090524, -1.443836447538996204 ) ) ;
#11613=CARTESIAN_POINT ( 'NONE',  ( -1.242826169824672977, 21.35102975155811222, 11.49999999999999645 ) ) ;
#11614=ORIENTED_EDGE ( 'NONE', *, *, #45777, .T. ) ;
#11617=CARTESIAN_POINT ( 'NONE',  ( -12.31279356157217109, -18.55646752483835016, 11.49999999999998934 ) ) ;
#11618=B_SPLINE_CURVE_WITH_KNOTS ( 'NONE', 3,
 ( #80377, #65678, #57059, #41318 ),
 .UNSPECIFIED., .F., .F.,
 ( 4, 4 ),
 ( 0.000000000000000000, 9.999999999998206125E-05 ),
 .UNSPECIFIED. ) ;
#11619=CARTESIAN_POINT ( 'NONE',  ( -20.66316395829706209, -0.6310838753663271516, -1.500000000000002220 ) ) ;
#11620=EDGE_LOOP ( 'NONE', ( #22443, #94601, #60277, #25483 ) ) ;
#11621=AXIS2_PLACEMENT_3D ( 'NONE', #5039, #44604, #45607 ) ;
#11625=ORIENTED_EDGE ( 'NONE', *, *, #50802, .F. ) ;
#11626=CARTESIAN_POINT ( 'NONE',  ( -50.04601614386864838, -25.10935134884508813, 2.868514420169689494 ) ) ;
#11627=CARTESIAN_POINT ( 'NONE',  ( 17.97375762979478253, -10.76934015532128797, -1.500000000000002220 ) ) ;
#11629=CARTESIAN_POINT ( 'NONE',  ( 3.414333255021221092, 21.62243999391013105, 11.49999999999999645 ) ) ;
#11630=CARTESIAN_POINT ( 'NONE',  ( -73.54183095359555011, -24.51419770103157347, 9.386484678747175181 ) ) ;
#11631=CARTESIAN_POINT ( 'NONE',  ( -11.58057713800463162, -19.31455136971746001, 11.49999999999998934 ) ) ;
#11632=CARTESIAN_POINT ( 'NONE',  ( -3.961239394588834895, 20.55660451852329018, 11.49999999999998934 ) ) ;
#11633=CARTESIAN_POINT ( 'NONE',  ( -90.52287095715006160, -29.50248528299804818, 1.056150453629040253 ) ) ;
#11634=CARTESIAN_POINT ( 'NONE',  ( -80.52287095715006160, -24.99132157543083821, 2.256160258750667502 ) ) ;
#11635=CARTESIAN_POINT ( 'NONE',  ( -29.62287095715006657, -24.27350855396620943, 9.819127054472291505 ) ) ;
#11637=VERTEX_POINT ( 'NONE', #49157 ) ;
#11642=ADVANCED_FACE ( 'NONE', ( #62365 ), #50142, .F. ) ;
#11645=CARTESIAN_POINT ( 'NONE',  ( 21.22668844964908885, 3.412186807495566132, -1.500000000000002220 ) ) ;
#11646=DIRECTION ( 'NONE',  ( 3.773278334444166432E-23, -1.000000000000000000, 0.000000000000000000 ) ) ;
#11647=CARTESIAN_POINT ( 'NONE',  ( 20.99878002148846790, -2.064974809011826729, 11.49999999999998934 ) ) ;
#11651=FACE_OUTER_BOUND ( 'NONE', #4029, .T. ) ;
#11652=CARTESIAN_POINT ( 'NONE',  ( -51.52287095715006870, -23.48786465467241058, 11.44779295918255002 ) ) ;
#11653=CARTESIAN_POINT ( 'NONE',  ( -9.261969182712835646, 20.05037652441878038, -1.500000000000002220 ) ) ;
#11655=CARTESIAN_POINT ( 'NONE',  ( -116.6272965939264594, -23.96119346886881729, -0.6495511937831833782 ) ) ;
#11657=DIRECTION ( 'NONE',  ( 0.000000000000000000, 0.9999999999976377785, 2.173523156925979975E-06 ) ) ;
#11658=CARTESIAN_POINT ( 'NONE',  ( -41.64605464260454681, -25.27955944056996884, 4.957686485891340311 ) ) ;
#11659=FACE_OUTER_BOUND ( 'NONE', #94636, .T. ) ;
#11663=CARTESIAN_POINT ( 'NONE',  ( -9.778911232092227124, -18.99720643767551209, -1.500000000000002220 ) ) ;
#11664=CARTESIAN_POINT ( 'NONE',  ( -69.27983724839798185, -25.13218956900901446, 7.108035130480557129 ) ) ;
#11665=CARTESIAN_POINT ( 'NONE',  ( -66.62287095715009855, -24.50216790748205753, 0.6166512839542495072 ) ) ;
#11666=CARTESIAN_POINT ( 'NONE',  ( -64.63656984362181390, -24.15620529776628445, 10.23563542870660115 ) ) ;
#11667=LINE ( 'NONE', #97410, #24852 ) ;
#11668=CARTESIAN_POINT ( 'NONE',  ( -3.649967738973055376, -22.27025559232234642, -1.500000000000002220 ) ) ;
#11669=CARTESIAN_POINT ( 'NONE',  ( -65.55620429048339304, -24.99156044556201905, 7.747789690856173195 ) ) ;
#11670=VERTEX_POINT ( 'NONE', #26795 ) ;
#11672=CARTESIAN_POINT ( 'NONE',  ( -18.76583335001664565, 6.068782795689376286, 11.49999999999999645 ) ) ;
#11673=CARTESIAN_POINT ( 'NONE',  ( -59.62287095715004881, -23.48783264082478794, -1.443836473390069042 ) ) ;
#11674=CARTESIAN_POINT ( 'NONE',  ( -32.07722060962682775, -24.86441978397624553, 8.247789967200544581 ) ) ;
#11678=CARTESIAN_POINT ( 'NONE',  ( -29.74701180552300883, -25.26026767148650265, 3.841291294183602378 ) ) ;
#11680=CARTESIAN_POINT ( 'NONE',  ( -16.54959454218438708, 13.92943311328891554, 11.49999999999998934 ) ) ;
#11682=CARTESIAN_POINT ( 'NONE',  ( -1.480291460309441920, -19.30061035156251847, -1.500000000000002220 ) ) ;
#11684=CARTESIAN_POINT ( 'NONE',  ( -97.52287095715006160, -23.47596703998600631, 11.44779298504228215 ) ) ;
#11685=CARTESIAN_POINT ( 'NONE',  ( -16.86558833231006460, 10.32443627698238409, -1.500000000000002220 ) ) ;
#11686=ADVANCED_FACE ( 'NONE', ( #66378 ), #72483, .T. ) ;
#11687=ORIENTED_EDGE ( 'NONE', *, *, #15552, .T. ) ;
#11688=CARTESIAN_POINT ( 'NONE',  ( 0.7435384974594729801, 20.27106041150680937, 11.49999999999999645 ) ) ;
#11690=ADVANCED_FACE ( 'NONE', ( #82570 ), #2976, .T. ) ;
#11691=B_SPLINE_CURVE_WITH_KNOTS ( 'NONE', 3,
 ( #163, #22974, #53964, #68684 ),
 .UNSPECIFIED., .F., .F.,
 ( 4, 4 ),
 ( 0.4901359185396870766, 0.4991423498118026658 ),
 .UNSPECIFIED. ) ;
#11692=ADVANCED_FACE ( 'NONE', ( #50632 ), #81084, .T. ) ;
#11693=VECTOR ( 'NONE', #62722, 1000.000000000000114 ) ;
#11698=CARTESIAN_POINT ( 'NONE',  ( -44.55620429048339304, -24.64965694238574656, 8.947790433994203596 ) ) ;
#11699=CARTESIAN_POINT ( 'NONE',  ( -96.52287095715010423, -23.48783264082477018, -1.443836473390086139 ) ) ;
#11700=CARTESIAN_POINT ( 'NONE',  ( 11.39338536883839659, -16.50304575528446804, -1.500000000000002220 ) ) ;
#11701=B_SPLINE_CURVE_WITH_KNOTS ( 'NONE', 3,
 ( #80722, #27929, #89828, #51269 ),
 .UNSPECIFIED., .F., .F.,
 ( 4, 4 ),
 ( 1.387778780781445521E-17, 9.999999999997510880E-05 ),
 .UNSPECIFIED. ) ;
#11704=CARTESIAN_POINT ( 'NONE',  ( -50.38822539166533687, -25.26258885410247856, 4.736250640224078268 ) ) ;
#11705=AXIS2_PLACEMENT_3D ( 'NONE', #21042, #97677, #98665 ) ;
#11706=CARTESIAN_POINT ( 'NONE',  ( -127.5228709571500900, -24.50216790748205398, 0.6166512839542636071 ) ) ;
#11708=AXIS2_PLACEMENT_3D ( 'NONE', #94570, #2240, #47907 ) ;
#11710=CARTESIAN_POINT ( 'NONE',  ( -73.50728567005882041, -24.15543982623907127, -0.2315651400026654816 ) ) ;
#11714=EDGE_LOOP ( 'NONE', ( #96887, #74365, #98346, #41545 ) ) ;
#11716=CARTESIAN_POINT ( 'NONE',  ( -19.77321833943668850, 4.698914572609424134, 11.49999999999998934 ) ) ;
#11717=ORIENTED_EDGE ( 'NONE', *, *, #40787, .T. ) ;
#11718=CARTESIAN_POINT ( 'NONE',  ( -18.54830753475928518, 13.48922247889305837, -1.500000000000002220 ) ) ;
#11719=CARTESIAN_POINT ( 'NONE',  ( -32.57079420858853780, -23.48783264082477729, -1.443836473390076147 ) ) ;
#11722=CARTESIAN_POINT ( 'NONE',  ( -108.5228709571500616, -23.48786465467241769, 11.44779295918253936 ) ) ;
#11727=CARTESIAN_POINT ( 'NONE',  ( -20.47598858559898716, 5.595549388561865456, 11.49999999999999645 ) ) ;
#11729=CARTESIAN_POINT ( 'NONE',  ( 13.47465251475156656, -17.59220275312388182, 11.49999999999998934 ) ) ;
#11730=CARTESIAN_POINT ( 'NONE',  ( 1.582324178664715975, -20.54890914157308401, -1.500000000000002220 ) ) ;
#11731=ORIENTED_EDGE ( 'NONE', *, *, #54621, .F. ) ;
#11732=CARTESIAN_POINT ( 'NONE',  ( -41.52202774044425126, -23.48783264082477729, -1.443836473390076147 ) ) ;
#11733=VECTOR ( 'NONE', #4456, 1000.000000000000114 ) ;
#11735=FACE_OUTER_BOUND ( 'NONE', #36249, .T. ) ;
#11736=CARTESIAN_POINT ( 'NONE',  ( -77.55620429048342146, -23.47593901973091235, -1.443836447539004642 ) ) ;
#11737=VERTEX_POINT ( 'NONE', #65884 ) ;
#11738=EDGE_LOOP ( 'NONE', ( #23072, #55116, #97609, #74471 ) ) ;
#11739=VERTEX_POINT ( 'NONE', #96806 ) ;
#11740=VECTOR ( 'NONE', #11524, 1000.000000000000114 ) ;
#11741=CARTESIAN_POINT ( 'NONE',  ( -77.52287095715007581, -23.73934037231757088, 11.05740245334329330 ) ) ;
#11744=CARTESIAN_POINT ( 'NONE',  ( 15.70846742882596025, 13.54617332914617478, -1.500000000000002220 ) ) ;
#11746=CARTESIAN_POINT ( 'NONE',  ( -12.78816955685674372, 17.57309652720472570, 11.49999999999999645 ) ) ;
#11747=ORIENTED_EDGE ( 'NONE', *, *, #91909, .F. ) ;
#11749=CARTESIAN_POINT ( 'NONE',  ( -115.5883540308789037, -24.73486907724917927, 1.287355809206966573 ) ) ;
#11750=CARTESIAN_POINT ( 'NONE',  ( -20.38924965233672282, -9.335317855073830273, 11.49999999999998934 ) ) ;
#11752=CARTESIAN_POINT ( 'NONE',  ( -104.5228709571500758, -29.50250786944525672, 11.44777988621623166 ) ) ;
#11753=ORIENTED_EDGE ( 'NONE', *, *, #96875, .T. ) ;
#11754=CARTESIAN_POINT ( 'NONE',  ( -31.52287095715006160, -29.50250786944525672, 11.44777988621624409 ) ) ;
#11755=CARTESIAN_POINT ( 'NONE',  ( -129.6228709571500417, -24.64898659630367916, 1.056161002820834804 ) ) ;
#11756=B_SPLINE_SURFACE_WITH_KNOTS ( 'NONE', 3, 1, ( 
 ( #15233, #78119 ),
 ( #31966, #93351 ),
 ( #77121, #46191 ),
 ( #38577, #54815 ),
 ( #61428, #38070 ),
 ( #99952, #7121 ),
 ( #92356, #39073 ),
 ( #99460, #53309 ),
 ( #70530, #8135 ),
 ( #22826, #84242 ),
 ( #30463, #93857 ),
 ( #23843, #54317 ),
 ( #53813, #14728 ),
 ( #69026, #512 ),
 ( #77622, #30959 ) ),
 .UNSPECIFIED., .F., .F., .F.,
 ( 4, 1, 1, 1, 1, 1, 1, 1, 1, 1, 1, 1, 4 ),
 ( 2, 2 ),
 ( 0.000000000000000000, 0.09870219630615274797, 0.1956723088106625263, 0.2924224265079539697, 0.3913425437998249712, 0.4444624406718897247, 0.5042287754493163243, 0.5703523379946782157, 0.6425457530977494169, 0.7222875053440166448, 0.8079211226827099912, 0.9004695379850130577, 1.000000000000000000 ),
 ( 0.000000000000000000, 1.000000000000000000 ),
 .UNSPECIFIED. ) ;
#11757=VERTEX_POINT ( 'NONE', #73970 ) ;
#11760=EDGE_CURVE ( 'NONE', #13388, #71512, #9618, .T. ) ;
#11763=CARTESIAN_POINT ( 'NONE',  ( 9.569808575145499319, 19.01914523534739132, -1.500000000000002220 ) ) ;
#11764=ADVANCED_FACE ( 'NONE', ( #61753 ), #92672, .T. ) ;
#11766=CARTESIAN_POINT ( 'NONE',  ( -100.7772468432415707, -25.12925546383932840, 7.065654974209207850 ) ) ;
#11768=CARTESIAN_POINT ( 'NONE',  ( 19.17057494584436839, 10.47865234463220396, 11.49999999999998934 ) ) ;
#11769=CARTESIAN_POINT ( 'NONE',  ( -68.62287095715005592, -29.50248528299804818, 1.056150453629036701 ) ) ;
#11770=CARTESIAN_POINT ( 'NONE',  ( -2.225104987405961854, -22.55768739424384606, -1.500000000000002220 ) ) ;
#11771=B_SPLINE_CURVE_WITH_KNOTS ( 'NONE', 3,
 ( #3910, #98222, #49582, #89134 ),
 .UNSPECIFIED., .F., .F.,
 ( 4, 4 ),
 ( 0.000000000000000000, 8.203125000004474199E-05 ),
 .UNSPECIFIED. ) ;
#11772=CARTESIAN_POINT ( 'NONE',  ( -41.24137195392557942, -25.18430942371155723, 3.620794074174289445 ) ) ;
#11774=CARTESIAN_POINT ( 'NONE',  ( -16.30586240431254197, 14.59307310709210626, -1.500000000000002220 ) ) ;
#11776=ORIENTED_EDGE ( 'NONE', *, *, #38663, .T. ) ;
#11777=CARTESIAN_POINT ( 'NONE',  ( -57.62287095715004881, -23.48783264082478794, -1.443836473390068820 ) ) ;
#11779=EDGE_CURVE ( 'NONE', #8368, #27242, #39793, .T. ) ;
#11780=ADVANCED_FACE ( 'NONE', ( #68851 ), #99769, .F. ) ;
#11781=ORIENTED_EDGE ( 'NONE', *, *, #7617, .F. ) ;
#11782=CARTESIAN_POINT ( 'NONE',  ( -30.63575758404999760, -23.78094912398190885, -0.9704635207981300304 ) ) ;
#11783=VERTEX_POINT ( 'NONE', #22153 ) ;
#11785=CARTESIAN_POINT ( 'NONE',  ( -43.52287095715006160, -29.50248528299804818, 1.056150453629031594 ) ) ;
#11786=CARTESIAN_POINT ( 'NONE',  ( -20.39836507935772403, -24.35390822839723768, 2.712351064733613537 ) ) ;
#11787=CARTESIAN_POINT ( 'NONE',  ( -3.310264809446246570, -21.00426241492911927, -1.500000000000002220 ) ) ;
#11789=CARTESIAN_POINT ( 'NONE',  ( -26.36141581567544989, -24.75186187578922414, 3.275178188152123582 ) ) ;
#11790=CARTESIAN_POINT ( 'NONE',  ( -85.50610730149335836, -24.40034930558991277, 0.3402023900116044608 ) ) ;
#11791=CARTESIAN_POINT ( 'NONE',  ( -68.51606564171095215, -23.73766607897670156, -1.055555164236458232 ) ) ;
#11792=CARTESIAN_POINT ( 'NONE',  ( -39.62287095715005592, -23.96177878511307568, 10.65340807706330395 ) ) ;
#11794=CARTESIAN_POINT ( 'NONE',  ( -6.365771329251782795, -18.49506561991874065, 11.49999999999999645 ) ) ;
#11795=CARTESIAN_POINT ( 'NONE',  ( -66.62287095715005592, -24.66019654487199020, 8.947790411086131712 ) ) ;
#11796=CARTESIAN_POINT ( 'NONE',  ( -28.59333068889780449, -24.76832095785427157, 8.029868342524341784 ) ) ;
#11798=DIRECTION ( 'NONE',  ( 0.000000000000000000, -2.173523156925979552E-06, 0.9999999999976378895 ) ) ;
#11799=CARTESIAN_POINT ( 'NONE',  ( -99.53504363246379683, -25.25095857004948385, 5.566583656979581463 ) ) ;
#11801=VECTOR ( 'NONE', #23277, 1000.000000000000114 ) ;
#11802=CARTESIAN_POINT ( 'NONE',  ( -81.73829046040381741, -25.24813826291026686, 6.803917685027681905 ) ) ;
#11803=EDGE_CURVE ( 'NONE', #60161, #9998, #19317, .T. ) ;
#11804=CARTESIAN_POINT ( 'NONE',  ( 17.66836560233463516, 8.693963128369697202, -1.500000000000002220 ) ) ;
#11806=ORIENTED_EDGE ( 'NONE', *, *, #68557, .T. ) ;
#11807=B_SPLINE_CURVE_WITH_KNOTS ( 'NONE', 3,
 ( #21256, #4564, #4060, #90287 ),
 .UNSPECIFIED., .F., .F.,
 ( 4, 4 ),
 ( 0.000000000000000000, 0.002094050480769230060 ),
 .UNSPECIFIED. ) ;
#11808=DIRECTION ( 'NONE',  ( 0.000000000000000000, -2.173523156925980399E-06, 0.9999999999976378895 ) ) ;
#11810=AXIS2_PLACEMENT_3D ( 'NONE', #95314, #72488, #20175 ) ;
#11813=CARTESIAN_POINT ( 'NONE',  ( -54.52287095715006870, -23.47596703998600631, 11.44779298504229104 ) ) ;
#11814=PLANE ( 'NONE',  #53950 ) ;
#11815=CARTESIAN_POINT ( 'NONE',  ( -47.59345066694555015, -24.15543982623907127, -0.2315651400026536022 ) ) ;
#11817=CARTESIAN_POINT ( 'NONE',  ( -105.5228709571500616, -25.00158670708909980, 2.256160236439166411 ) ) ;
#11820=CARTESIAN_POINT ( 'NONE',  ( -50.62287095715005592, -24.99132157543083821, 2.256160258750667502 ) ) ;
#11821=CARTESIAN_POINT ( 'NONE',  ( 11.38277053702107899, 16.36964821499295653, 11.49999999999998934 ) ) ;
#11822=CARTESIAN_POINT ( 'NONE',  ( -0.006913265320916323065, -22.96050234768690856, 3.564872121755937151 ) ) ;
#11823=CARTESIAN_POINT ( 'NONE',  ( 8.615496892348360802, 17.92367856960711947, -1.500000000000002220 ) ) ;
#11825=CARTESIAN_POINT ( 'NONE',  ( -74.52287095715007581, -24.64898659630528854, 1.056161002820824368 ) ) ;
#11826=DIRECTION ( 'NONE',  ( -3.773278334453079030E-23, 0.9999999999976377785, 2.173523156925979128E-06 ) ) ;
#11828=CARTESIAN_POINT ( 'NONE',  ( -72.62287095715004170, -23.48786465467241058, 11.44779295918254647 ) ) ;
#11829=LINE ( 'NONE', #81848, #28933 ) ;
#11833=B_SPLINE_SURFACE_WITH_KNOTS ( 'NONE', 3, 3, ( 
 ( #47877, #79309, #88437, #94036 ),
 ( #18910, #63109, #49891, #40261 ),
 ( #78796, #72216, #9805, #64629 ),
 ( #2708, #24521, #34156, #65123 ),
 ( #57000, #80824, #18420, #71211 ),
 ( #1706, #10307, #55489, #49389 ),
 ( #33650, #86925, #79809, #80318 ) ),
 .UNSPECIFIED., .F., .F., .F.,
 ( 4, 3, 4 ),
 ( 4, 4 ),
 ( 0.0004766839783839991324, 0.1029713700210907190, 0.2054660560637974476 ),
 ( 0.4095981920303961021, 0.4107999044396243304 ),
 .UNSPECIFIED. ) ;
#11834=CARTESIAN_POINT ( 'NONE',  ( -62.62287095715004881, -24.64898659630528854, 1.056161002820822592 ) ) ;
#11835=CARTESIAN_POINT ( 'NONE',  ( -127.6236467198321805, -24.51314013834317151, 0.6176544820404252789 ) ) ;
#11837=CARTESIAN_POINT ( 'NONE',  ( -2.479824388263708990, 20.08073137130260122, 11.49999999999998934 ) ) ;
#11839=CARTESIAN_POINT ( 'NONE',  ( -112.6228709571500559, -29.50247984919015209, -1.443849546365048253 ) ) ;
#11840=VECTOR ( 'NONE', #71417, 1000.000000000000114 ) ;
#11841=ADVANCED_FACE ( 'NONE', ( #14553 ), #60255, .T. ) ;
#11842=EDGE_CURVE ( 'NONE', #16998, #48696, #99090, .T. ) ;
#11843=CARTESIAN_POINT ( 'NONE',  ( -109.6228709571500559, -24.64898659630368627, 1.056161002820831474 ) ) ;
#11844=ADVANCED_FACE ( 'NONE', ( #53641 ), #99287, .F. ) ;
#11846=CARTESIAN_POINT ( 'NONE',  ( -46.62287095715004170, -23.72773821059535138, 11.05748984161097503 ) ) ;
#11848=CARTESIAN_POINT ( 'NONE',  ( -6.237196068801617699, -19.06703463882530158, -1.500000000000002220 ) ) ;
#11850=CARTESIAN_POINT ( 'NONE',  ( -6.845587600281468177, 19.88882266644084496, 11.49999999999999645 ) ) ;
#11853=CARTESIAN_POINT ( 'NONE',  ( -70.55922311016780668, -23.85049219812685806, 10.88485053497527311 ) ) ;
#11854=CARTESIAN_POINT ( 'NONE',  ( 11.82310115920509830, 18.66461490495635545, 11.49999999999998934 ) ) ;
#11855=CARTESIAN_POINT ( 'NONE',  ( -40.11299260137283795, -25.27806099098225090, 5.047402397866858514 ) ) ;
#11856=DIRECTION ( 'NONE',  ( -3.773278334453079618E-23, 0.9999999999976377785, 2.173523156925979975E-06 ) ) ;
#11858=FACE_OUTER_BOUND ( 'NONE', #35810, .T. ) ;
#11860=ORIENTED_EDGE ( 'NONE', *, *, #7905, .T. ) ;
#11863=B_SPLINE_CURVE_WITH_KNOTS ( 'NONE', 3,
 ( #52273, #36536, #19806, #89338 ),
 .UNSPECIFIED., .F., .F.,
 ( 4, 4 ),
 ( 0.4308076291828551452, 0.4398140604549706789 ),
 .UNSPECIFIED. ) ;
#11865=LINE ( 'NONE', #57565, #32533 ) ;
#11866=CARTESIAN_POINT ( 'NONE',  ( 18.80685554986811070, -8.408966509905500430, -1.500000000000002220 ) ) ;
#11868=CARTESIAN_POINT ( 'NONE',  ( 21.48638754631891246, 1.654510534108022179, 11.49999999999999645 ) ) ;
#11870=DIRECTION ( 'NONE',  ( 0.000000000000000000, -0.9999999999976377785, -2.173523156925979128E-06 ) ) ;
#11873=CARTESIAN_POINT ( 'NONE',  ( -2.938769918389303459, -22.12206158279486345, 11.49999999999998934 ) ) ;
#11877=EDGE_CURVE ( 'NONE', #79347, #97718, #55645, .T. ) ;
#11878=VERTEX_POINT ( 'NONE', #77937 ) ;
#11879=CARTESIAN_POINT ( 'NONE',  ( -101.6228709571500701, -23.96127896941631619, -0.6493128931037793761 ) ) ;
#11881=CARTESIAN_POINT ( 'NONE',  ( 4.135342931496230001, -20.44547621892628797, -1.500000000000002220 ) ) ;
#11882=ORIENTED_EDGE ( 'NONE', *, *, #51604, .T. ) ;
#11883=CARTESIAN_POINT ( 'NONE',  ( -39.08733197973624840, -25.25129735365466388, 3.851328594451885134 ) ) ;
#11885=EDGE_LOOP ( 'NONE', ( #38242, #60679, #35838, #14510 ) ) ;
#11886=ORIENTED_EDGE ( 'NONE', *, *, #65677, .T. ) ;
#11888=CARTESIAN_POINT ( 'NONE',  ( -50.65607660699232895, -25.30191415566046587, 4.703207432804873633 ) ) ;
#11889=CARTESIAN_POINT ( 'NONE',  ( 13.75562813033083742, -15.94169299924578453, -1.500000000000002220 ) ) ;
#11891=CARTESIAN_POINT ( 'NONE',  ( -114.6228709571500559, -24.64965695001469115, 8.947790433994176951 ) ) ;
#11893=CARTESIAN_POINT ( 'NONE',  ( -120.5539051758846085, -24.52399227489125266, 9.353111116836528183 ) ) ;
#11895=CARTESIAN_POINT ( 'NONE',  ( -81.42380231474228935, -25.30401792888237011, 5.197789011716578145 ) ) ;
#11896=FACE_OUTER_BOUND ( 'NONE', #29518, .T. ) ;
#11897=CARTESIAN_POINT ( 'NONE',  ( -18.02536786162489335, -12.12045427182966861, -1.500000000000002220 ) ) ;
#11899=CARTESIAN_POINT ( 'NONE',  ( -19.27636426328722763, -11.15942449563467775, 11.49999999999999645 ) ) ;
#11900=VERTEX_POINT ( 'NONE', #17054 ) ;
#11901=CARTESIAN_POINT ( 'NONE',  ( -72.62287095715004170, -23.48786465467241058, 11.44779295918254647 ) ) ;
#11902=B_SPLINE_CURVE_WITH_KNOTS ( 'NONE', 3,
 ( #21389, #83804, #14284, #61486, #31017, #37631, #13783, #99513, #69080, #68094, #52867, #67601, #68589, #44260, #75189, #84297, #52366, #77177 ),
 .UNSPECIFIED., .F., .F.,
 ( 4, 2, 2, 2, 2, 2, 2, 2, 4 ),
 ( 0.000000000000000000, 0.0002613877182136167495, 0.0005227754364272334990, 0.0007841631546408503028, 0.001045550872854466998, 0.001306938591068083693, 0.001568326309281700606, 0.001829714027495317301, 0.002091101745708933996 ),
 .UNSPECIFIED. ) ;
#11906=ORIENTED_EDGE ( 'NONE', *, *, #50651, .T. ) ;
#11908=CARTESIAN_POINT ( 'NONE',  ( -40.62287095715008434, -24.92579138211018730, 1.929029949965663349 ) ) ;
#11909=VERTEX_POINT ( 'NONE', #62248 ) ;
#11910=VERTEX_POINT ( 'NONE', #1846 ) ;
#11911=CARTESIAN_POINT ( 'NONE',  ( -75.52287095715007581, -24.83602698348160942, 1.605859176311265069 ) ) ;
#11912=B_SPLINE_CURVE_WITH_KNOTS ( 'NONE', 3,
 ( #46674, #40056, #22307, #24322, #93836, #7598, #77597, #53285, #8101, #38550, #39050, #78094, #8608, #39553 ),
 .UNSPECIFIED., .F., .F.,
 ( 4, 2, 2, 2, 2, 2, 4 ),
 ( 0.000000000000000000, 0.0001870305922025326481, 0.0003740611844050652961, 0.0007481223688101111850, 0.001122183553215157182, 0.001309214145417679585, 0.001496244737620201770 ),
 .UNSPECIFIED. ) ;
#11913=CARTESIAN_POINT ( 'NONE',  ( -64.52287095715006160, -24.64898659630528854, 1.056161002820822592 ) ) ;
#11914=B_SPLINE_CURVE_WITH_KNOTS ( 'NONE', 3,
 ( #1517, #61034, #91965, #40578 ),
 .UNSPECIFIED., .F., .F.,
 ( 4, 4 ),
 ( 0.000000000000000000, 9.999999999998897304E-05 ),
 .UNSPECIFIED. ) ;
#11918=CARTESIAN_POINT ( 'NONE',  ( -130.5728709571501156, -24.38618449965941082, 9.939220798225495201 ) ) ;
#11919=CARTESIAN_POINT ( 'NONE',  ( 1.585521478320181865, 22.38520322874704149, -1.500000000000002220 ) ) ;
#11920=VERTEX_POINT ( 'NONE', #85566 ) ;
#11923=CARTESIAN_POINT ( 'NONE',  ( -101.5932190732468712, -23.96169478059713853, 10.65365249895717881 ) ) ;
#11926=CARTESIAN_POINT ( 'NONE',  ( -130.5728709571500588, -24.66513809378597344, 8.909134979017300893 ) ) ;
#11927=CARTESIAN_POINT ( 'NONE',  ( -5.058734511472819051, -18.94576116945722788, -1.500000000000002220 ) ) ;
#11930=VERTEX_POINT ( 'NONE', #48528 ) ;
#11931=CARTESIAN_POINT ( 'NONE',  ( 15.50980990363467882, 14.95361599516425244, 11.49999999999998934 ) ) ;
#11933=CARTESIAN_POINT ( 'NONE',  ( -71.23336565260535735, -25.12219025383727455, 6.552467362938464213 ) ) ;
#11934=CARTESIAN_POINT ( 'NONE',  ( -32.99388727629348494, -29.50248914092071928, 2.831113219569932227 ) ) ;
#11935=DIRECTION ( 'NONE',  ( -3.773278334453079618E-23, 0.9999999999976377785, 2.173523156925978705E-06 ) ) ;
#11936=CARTESIAN_POINT ( 'NONE',  ( 22.97298546869389568, 1.202750762487129199, -1.500000000000002220 ) ) ;
#11939=CARTESIAN_POINT ( 'NONE',  ( -49.61440498689717060, -23.48783264082477018, -1.443836473390093911 ) ) ;
#11940=CARTESIAN_POINT ( 'NONE',  ( -4.889416449700032530, -19.50743224814450016, 11.49999999999999645 ) ) ;
#11942=LINE ( 'NONE', #58626, #32272 ) ;
#11944=DIRECTION ( 'NONE',  ( -3.773278334444166432E-23, 1.000000000000000000, 0.000000000000000000 ) ) ;
#11945=DIRECTION ( 'NONE',  ( -1.000000000000000000, -3.773278334444166432E-23, -8.201307841325785021E-29 ) ) ;
#11946=CARTESIAN_POINT ( 'NONE',  ( -13.56193660873917395, -14.51407242162769151, -1.500000000000002220 ) ) ;
#11947=CARTESIAN_POINT ( 'NONE',  ( -113.5154190852081797, -24.51314013834315375, 0.6176544820404169522 ) ) ;
#11948=CARTESIAN_POINT ( 'NONE',  ( -9.502044936771568473, -17.27029980899984452, -1.500000000000002220 ) ) ;
#11949=CARTESIAN_POINT ( 'NONE',  ( -91.12544711349063675, -25.37321702313245453, 5.213201572634361014 ) ) ;
#11951=FACE_OUTER_BOUND ( 'NONE', #62292, .T. ) ;
#11952=CARTESIAN_POINT ( 'NONE',  ( -79.52287095715006160, -24.64965694238575011, 8.947790433994198267 ) ) ;
#11953=CARTESIAN_POINT ( 'NONE',  ( -0.003042231299257275486, -20.61035990087709635, 11.49999999999999645 ) ) ;
#11956=CARTESIAN_POINT ( 'NONE',  ( -16.08347380570801377, -15.98036338121420030, 11.49999999999999645 ) ) ;
#11961=EDGE_CURVE ( 'NONE', #77504, #28708, #78445, .T. ) ;
#11963=EDGE_CURVE ( 'NONE', #66746, #65800, #8344, .T. ) ;
#11964=CARTESIAN_POINT ( 'NONE',  ( -26.98635835925963633, -24.93063604734380689, 8.112878671671195363 ) ) ;
#11965=EDGE_CURVE ( 'NONE', #69536, #9262, #16800, .T. ) ;
#11966=CARTESIAN_POINT ( 'NONE',  ( -104.6228709571500559, -29.50248528299804818, 1.056150453629042030 ) ) ;
#11968=ORIENTED_EDGE ( 'NONE', *, *, #15557, .F. ) ;
#11969=ADVANCED_FACE ( 'NONE', ( #47521 ), #7942, .T. ) ;
#11970=ORIENTED_EDGE ( 'NONE', *, *, #1033, .T. ) ;
#11972=CARTESIAN_POINT ( 'NONE',  ( 18.61037501828884189, -13.27421459584354579, 11.49999999999998934 ) ) ;
#11974=CARTESIAN_POINT ( 'NONE',  ( 21.29926025483437257, -3.289820829717503337, -1.500000000000002220 ) ) ;
#11977=CARTESIAN_POINT ( 'NONE',  ( -21.69688529672534827, 6.072505851105969299, 11.49999999999999645 ) ) ;
#11978=VERTEX_POINT ( 'NONE', #33278 ) ;
#11979=LINE ( 'NONE', #94714, #59490 ) ;
#11980=CARTESIAN_POINT ( 'NONE',  ( 3.092608977599853315, -21.74436839971096802, -1.500000000000002220 ) ) ;
#11982=DIRECTION ( 'NONE',  ( 0.000000000000000000, -0.9999999999976377785, -2.173523156925979975E-06 ) ) ;
#11984=CARTESIAN_POINT ( 'NONE',  ( -28.62287095715004881, -23.31957264754183967, 11.44779298504227860 ) ) ;
#11987=DIRECTION ( 'NONE',  ( 1.000000000000000000, 3.773278334444166432E-23, 8.201307841325785021E-29 ) ) ;
#11988=VERTEX_POINT ( 'NONE', #94175 ) ;
#11989=VERTEX_POINT ( 'NONE', #64266 ) ;
#11992=DIRECTION ( 'NONE',  ( -1.000000000000000000, -3.773278334444167608E-23, -8.201307833595939069E-29 ) ) ;
#11994=CARTESIAN_POINT ( 'NONE',  ( 13.37706023731332827, -15.40713922116925616, -1.500000000000002220 ) ) ;
#11997=CARTESIAN_POINT ( 'NONE',  ( -70.95580061108532277, -25.06113984836056119, 7.428384239504691067 ) ) ;
#11998=FACE_OUTER_BOUND ( 'NONE', #45787, .T. ) ;
#11999=CARTESIAN_POINT ( 'NONE',  ( -105.5186488368198496, -23.85016227208580730, -0.8807180028928328630 ) ) ;
#12000=CARTESIAN_POINT ( 'NONE',  ( -71.70128661679227378, -25.03149591267348484, 6.373708887022837111 ) ) ;
#12002=ORIENTED_EDGE ( 'NONE', *, *, #99846, .F. ) ;
#12003=CARTESIAN_POINT ( 'NONE',  ( -28.45618646431091392, -25.21531712953401083, 2.526464341324828666 ) ) ;
#12004=CARTESIAN_POINT ( 'NONE',  ( -87.62287095715004170, -23.47593901973091235, -1.443836447539002865 ) ) ;
#12007=CARTESIAN_POINT ( 'NONE',  ( -8.830788454959730416, 18.81286502489961876, 11.49999999999998934 ) ) ;
#12009=ORIENTED_EDGE ( 'NONE', *, *, #6101, .T. ) ;
#12011=EDGE_LOOP ( 'NONE', ( #62169, #54783, #96226, #2909 ) ) ;
#12014=ORIENTED_EDGE ( 'NONE', *, *, #90736, .F. ) ;
#12015=ORIENTED_EDGE ( 'NONE', *, *, #2752, .F. ) ;
#12016=PLANE ( 'NONE',  #29944 ) ;
#12019=CARTESIAN_POINT ( 'NONE',  ( -70.46019744876114999, -25.24515042775860962, 5.316128055210258552 ) ) ;
#12020=CARTESIAN_POINT ( 'NONE',  ( 19.90762846840230083, -9.494064324355022677, 11.49999999999999645 ) ) ;
#12023=CARTESIAN_POINT ( 'NONE',  ( 16.66146196086182130, -15.28366505690825328, 11.49999999999998934 ) ) ;
#12024=EDGE_CURVE ( 'NONE', #53428, #64023, #66435, .T. ) ;
#12025=DIRECTION ( 'NONE',  ( 0.000000000000000000, -0.9999999999976377785, -2.173523156925979128E-06 ) ) ;
#12027=ORIENTED_EDGE ( 'NONE', *, *, #31718, .T. ) ;
#12028=CARTESIAN_POINT ( 'NONE',  ( -120.6228709571500417, -29.50250786944525672, 11.44777988621622811 ) ) ;
#12030=B_SPLINE_SURFACE_WITH_KNOTS ( 'NONE', 3, 3, ( 
 ( #82562, #13044, #13541, #5441 ),
 ( #75436, #5936, #36892, #67856 ),
 ( #98777, #29277, #91172, #52619 ),
 ( #83555, #53132, #45517, #31271 ),
 ( #99762, #16536, #84557, #39887 ),
 ( #94168, #325, #76932, #62240 ),
 ( #30775, #15542, #30268, #93160 ) ),
 .UNSPECIFIED., .F., .F., .F.,
 ( 4, 3, 4 ),
 ( 4, 4 ),
 ( 0.7945040050992238090, 0.8970133687736498995, 0.9995227324480758790 ),
 ( 0.3395802893024847946, 0.3407497866532611663 ),
 .UNSPECIFIED. ) ;
#12031=FACE_OUTER_BOUND ( 'NONE', #58687, .T. ) ;
#12032=VERTEX_POINT ( 'NONE', #47018 ) ;
#12033=CARTESIAN_POINT ( 'NONE',  ( -3.044128750896296420, -20.94304649679510888, 11.49999999999998934 ) ) ;
#12034=LINE ( 'NONE', #66352, #70271 ) ;
#12036=CARTESIAN_POINT ( 'NONE',  ( 15.88595335714125589, -15.59144682577495189, -1.500000000000002220 ) ) ;
#12037=CARTESIAN_POINT ( 'NONE',  ( -46.62287095715006302, -24.33832256526968862, 0.1851278514119869822 ) ) ;
#12038=ORIENTED_EDGE ( 'NONE', *, *, #58278, .T. ) ;
#12039=CARTESIAN_POINT ( 'NONE',  ( -78.52287095715006160, -23.47593901973090169, -1.443836447538996648 ) ) ;
#12040=CARTESIAN_POINT ( 'NONE',  ( -96.52287095715006160, -29.50248528299804818, 1.056150453629042030 ) ) ;
#12042=CARTESIAN_POINT ( 'NONE',  ( -45.52287095715006160, -23.47596703998600631, 11.44779298504229104 ) ) ;
#12043=CARTESIAN_POINT ( 'NONE',  ( -19.43040671759091609, -1.856541507571394467, 11.49999999999998934 ) ) ;
#12044=CARTESIAN_POINT ( 'NONE',  ( 11.41860910855227829, 18.14899599152127152, -1.500000000000002220 ) ) ;
#12045=CARTESIAN_POINT ( 'NONE',  ( -26.06135888742384665, -24.92774869473493027, 2.563275193131095087 ) ) ;
#12046=DIRECTION ( 'NONE',  ( -3.773278334453079618E-23, 0.9999999999976377785, 2.173523156925979975E-06 ) ) ;
#12047=CARTESIAN_POINT ( 'NONE',  ( -77.55422962360664485, -23.96119346886880663, -0.6495511937832126881 ) ) ;
#12048=CARTESIAN_POINT ( 'NONE',  ( 21.14626179850551324, 8.528272852130310611, -1.500000000000002220 ) ) ;
#12050=CARTESIAN_POINT ( 'NONE',  ( -106.6321266654194631, -23.73791477778912551, 11.05961554403169878 ) ) ;
#12052=CARTESIAN_POINT ( 'NONE',  ( -5.841000908416043913, -19.03464889989004050, 11.49999999999999645 ) ) ;
#12053=DIRECTION ( 'NONE',  ( -1.000000000000000000, -3.773278334444166432E-23, -8.201307841325785021E-29 ) ) ;
#12054=CARTESIAN_POINT ( 'NONE',  ( -39.53338521000194561, -24.51419770103158413, 9.386484678747189392 ) ) ;
#12055=CARTESIAN_POINT ( 'NONE',  ( -101.6228709571500559, -24.33832256526968862, 0.1851278514119917562 ) ) ;
#12058=CARTESIAN_POINT ( 'NONE',  ( -62.62287095715009144, -24.33927499327853994, 9.819080762295820719 ) ) ;
#12060=CARTESIAN_POINT ( 'NONE',  ( -4.559408409702599307, -21.23122434433648209, 11.49999999999998934 ) ) ;
#12062=CARTESIAN_POINT ( 'NONE',  ( 3.994393897313025743, -19.14333888664780048, -1.500000000000002220 ) ) ;
#12065=CARTESIAN_POINT ( 'NONE',  ( -51.55620429048339304, -24.66019654487199020, 8.947790411086133489 ) ) ;
#12066=CARTESIAN_POINT ( 'NONE',  ( 20.41236503877875563, 1.188189311754236144, 11.49999999999999645 ) ) ;
#12068=DIRECTION ( 'NONE',  ( -1.000000000000000000, -3.773278334444167608E-23, -8.201307810031802745E-29 ) ) ;
#12071=CARTESIAN_POINT ( 'NONE',  ( -53.52287095715006870, -29.50250786944525672, 11.44777988621624054 ) ) ;
#12074=CARTESIAN_POINT ( 'NONE',  ( -35.52287095715006870, -29.50248789122583659, 2.256150453626215580 ) ) ;
#12075=EDGE_CURVE ( 'NONE', #19028, #8399, #34961, .T. ) ;
#12079=CARTESIAN_POINT ( 'NONE',  ( -16.20615075098634961, 16.30094363606528418, 11.49999999999999645 ) ) ;
#12080=CARTESIAN_POINT ( 'NONE',  ( -0.9122204482399535186, 22.77315974801211240, 11.49999999999998934 ) ) ;
#12082=EDGE_CURVE ( 'NONE', #43735, #58649, #84545, .T. ) ;
#12084=DIRECTION ( 'NONE',  ( -3.773278334444166432E-23, 1.000000000000000000, 0.000000000000000000 ) ) ;
#12086=CARTESIAN_POINT ( 'NONE',  ( -100.6814946224345846, -25.31267346029541443, 4.736250531364077254 ) ) ;
#12089=B_SPLINE_CURVE_WITH_KNOTS ( 'NONE', 3,
 ( #12452, #94820, #70998, #74355 ),
 .UNSPECIFIED., .F., .F.,
 ( 4, 4 ),
 ( 0.4490887540585746796, 0.4500895010993400946 ),
 .UNSPECIFIED. ) ;
#12090=CARTESIAN_POINT ( 'NONE',  ( -20.59625928752216240, -7.366027188055905839, -1.500000000000002220 ) ) ;
#12092=CARTESIAN_POINT ( 'NONE',  ( -101.5228709571500758, -24.65952944569304606, 1.056160979905702346 ) ) ;
#12095=VERTEX_POINT ( 'NONE', #43411 ) ;
#12096=CARTESIAN_POINT ( 'NONE',  ( -12.60687543931603471, -16.05746371069360379, 11.49999999999998934 ) ) ;
#12099=ORIENTED_EDGE ( 'NONE', *, *, #38903, .T. ) ;
#12100=ORIENTED_EDGE ( 'NONE', *, *, #39031, .T. ) ;
#12101=ADVANCED_FACE ( 'NONE', ( #41920 ), #26681, .F. ) ;
#12102=CARTESIAN_POINT ( 'NONE',  ( 13.09964176094197441, 18.96253433080681106, -1.500000000000002220 ) ) ;
#12103=CARTESIAN_POINT ( 'NONE',  ( -80.52287095715006160, -24.63287334234178871, 0.9662140553045349689 ) ) ;
#12104=CARTESIAN_POINT ( 'NONE',  ( 19.72175082351460063, -4.362005935662174316, -1.500000000000002220 ) ) ;
#12106=CARTESIAN_POINT ( 'NONE',  ( -45.62287095715004881, -29.50249982740957577, 7.747779886224967605 ) ) ;
#12108=CARTESIAN_POINT ( 'NONE',  ( -95.59106694108504598, -24.40034930558991633, 0.3402023900116099009 ) ) ;
#12109=CARTESIAN_POINT ( 'NONE',  ( -123.6228709571500559, -23.47593901973091235, -1.443836447538997536 ) ) ;
#12110=CARTESIAN_POINT ( 'NONE',  ( 19.36035776617087123, -9.008237321879198234, 11.49999999999999645 ) ) ;
#12113=ORIENTED_EDGE ( 'NONE', *, *, #79142, .T. ) ;
#12114=CARTESIAN_POINT ( 'NONE',  ( 7.309977242446557888, -21.02818303981469583, 11.49999999999998934 ) ) ;
#12115=CARTESIAN_POINT ( 'NONE',  ( 20.35908867758196550, 3.722869731652943770, 11.49999999999998934 ) ) ;
#12116=VECTOR ( 'NONE', #98051, 1000.000000000000114 ) ;
#12117=EDGE_LOOP ( 'NONE', ( #69412, #81162, #25936, #21205 ) ) ;
#12119=ORIENTED_EDGE ( 'NONE', *, *, #13693, .T. ) ;
#12120=CARTESIAN_POINT ( 'NONE',  ( -61.62287095715004881, -24.66019654487199020, 8.947790411086131712 ) ) ;
#12121=ORIENTED_EDGE ( 'NONE', *, *, #11803, .T. ) ;
#12122=CARTESIAN_POINT ( 'NONE',  ( -111.6468792378191779, -25.28710546256126790, 4.332404433089555695 ) ) ;
#12123=CARTESIAN_POINT ( 'NONE',  ( -19.40224465947428456, -7.824916089261592766, -1.500000000000002220 ) ) ;
#12124=CARTESIAN_POINT ( 'NONE',  ( -19.33260374144687077, -10.33727041909969380, 11.49999999999999645 ) ) ;
#12125=EDGE_CURVE ( 'NONE', #65481, #14129, #35791, .T. ) ;
#12127=CARTESIAN_POINT ( 'NONE',  ( -107.6228709571500701, -23.48786465467241769, 11.44779295918253936 ) ) ;
#12128=CARTESIAN_POINT ( 'NONE',  ( -1.797493081057526032, -22.44471576765463183, -1.500000000000002220 ) ) ;
#12129=CARTESIAN_POINT ( 'NONE',  ( 15.04517842881462819, -14.58609674458608829, -1.500000000000002220 ) ) ;
#12130=CARTESIAN_POINT ( 'NONE',  ( -26.27733073949819698, -24.88149021042581666, 6.353770771295153885 ) ) ;
#12132=B_SPLINE_CURVE_WITH_KNOTS ( 'NONE', 3,
 ( #32764, #93151, #76922, #31769 ),
 .UNSPECIFIED., .F., .F.,
 ( 4, 4 ),
 ( 1.387778780781445676E-17, 0.0001000000000000028779 ),
 .UNSPECIFIED. ) ;
#12133=CARTESIAN_POINT ( 'NONE',  ( -119.5193653822925484, -24.15620529776629510, 10.23563542870659582 ) ) ;
#12134=CARTESIAN_POINT ( 'NONE',  ( -99.52287095715009002, -23.47593901973090524, -1.443836447538996648 ) ) ;
#12138=CARTESIAN_POINT ( 'NONE',  ( -106.6228709571500559, -29.50250786944525672, 11.44777988621622988 ) ) ;
#12139=ORIENTED_EDGE ( 'NONE', *, *, #83089, .T. ) ;
#12140=CARTESIAN_POINT ( 'NONE',  ( 21.40653236543258231, -1.377805879665675803, -1.500000000000002220 ) ) ;
#12141=EDGE_CURVE ( 'NONE', #73698, #39531, #78609, .T. ) ;
#12142=CARTESIAN_POINT ( 'NONE',  ( -59.52287095715006160, -23.48783264082477018, -1.443836473390095021 ) ) ;
#12144=CARTESIAN_POINT ( 'NONE',  ( 19.39439428382967634, -8.317090367284466268, 11.49999999999998934 ) ) ;
#12147=CARTESIAN_POINT ( 'NONE',  ( -50.51068615954277874, -23.85049219812685095, 10.88485053497527133 ) ) ;
#12148=CARTESIAN_POINT ( 'NONE',  ( -80.84160375922890296, -25.30877089043013228, 4.579768006309718587 ) ) ;
#12150=B_SPLINE_CURVE_WITH_KNOTS ( 'NONE', 3,
 ( #13013, #13511, #66342, #97266, #28253, #83023, #44483, #50104, #73439, #75407 ),
 .UNSPECIFIED., .F., .F.,
 ( 4, 2, 2, 2, 4 ),
 ( 0.000000000000000000, 0.0001573231488620521995, 0.0003146462977241043990, 0.0004719694465861565985, 0.0006292925954482087979 ),
 .UNSPECIFIED. ) ;
#12151=CARTESIAN_POINT ( 'NONE',  ( 21.87352179494074633, -3.179377960941109915, -1.500000000000002220 ) ) ;
#12152=ORIENTED_EDGE ( 'NONE', *, *, #56853, .F. ) ;
#12153=B_SPLINE_CURVE_WITH_KNOTS ( 'NONE', 3,
 ( #73418, #90627, #88643, #90132 ),
 .UNSPECIFIED., .F., .F.,
 ( 4, 4 ),
 ( 0.000000000000000000, 0.002085937500000002720 ),
 .UNSPECIFIED. ) ;
#12157=CARTESIAN_POINT ( 'NONE',  ( -78.62287095715007013, -24.66019654487199375, 8.947790411086124607 ) ) ;
#12158=CARTESIAN_POINT ( 'NONE',  ( -28.39313913820096857, -25.15290109896971416, 6.075536601959948158 ) ) ;
#12161=CARTESIAN_POINT ( 'NONE',  ( 8.224165413489119558, 19.69228431130148493, -1.500000000000002220 ) ) ;
#12162=CARTESIAN_POINT ( 'NONE',  ( -68.98046560660316118, -25.21707011523245967, 6.550344061802529261 ) ) ;
#12163=CARTESIAN_POINT ( 'NONE',  ( -50.91671811657901969, -25.31392319263089519, 5.203681702801226550 ) ) ;
#12164=CARTESIAN_POINT ( 'NONE',  ( -86.58953762381671027, -24.64898659630528854, 1.056161002820827477 ) ) ;
#12165=DIRECTION ( 'NONE',  ( -3.773278334444167608E-23, 1.000000000000000000, 0.000000000000000000 ) ) ;
#12166=CARTESIAN_POINT ( 'NONE',  ( 16.59953334139655468, -15.42474913338910980, -1.500000000000002220 ) ) ;
#12167=CARTESIAN_POINT ( 'NONE',  ( -85.52287095715004739, -25.00158670708909625, 2.256160236439166411 ) ) ;
#12168=EDGE_LOOP ( 'NONE', ( #93349, #72278, #18499, #94724 ) ) ;
#12169=CARTESIAN_POINT ( 'NONE',  ( -35.62287095715004170, -24.15516710230296482, 10.28746687063729048 ) ) ;
#12171=CARTESIAN_POINT ( 'NONE',  ( -18.32884136524465291, -7.267937366463995907, 11.49999999999999645 ) ) ;
#12172=CARTESIAN_POINT ( 'NONE',  ( -73.62287095715005592, -23.47593901973091235, -1.443836447539006196 ) ) ;
#12173=CARTESIAN_POINT ( 'NONE',  ( -67.62721668323153779, -24.51314013834315730, 0.6176544820404126224 ) ) ;
#12175=CARTESIAN_POINT ( 'NONE',  ( -42.55620429048338593, -23.47593901973091235, -1.443836447539011525 ) ) ;
#12176=CARTESIAN_POINT ( 'NONE',  ( -28.79528301136424417, -25.26026362501326972, 1.979579709026720202 ) ) ;
#12177=CARTESIAN_POINT ( 'NONE',  ( -40.43756433397305727, -25.11033443737753501, 2.832404817301930056 ) ) ;
#12178=CARTESIAN_POINT ( 'NONE',  ( -21.57582672592670292, -1.461774377805347802, -1.500000000000002220 ) ) ;
#12180=CARTESIAN_POINT ( 'NONE',  ( -70.62287095715005592, -25.00158670708909270, 2.256160236439166855 ) ) ;
#12182=CARTESIAN_POINT ( 'NONE',  ( -71.52287095715007581, -29.50250786944525672, 11.44777988621623699 ) ) ;
#12183=CARTESIAN_POINT ( 'NONE',  ( -3.504374479207110316, 19.46862825742285708, -1.500000000000002220 ) ) ;
#12184=VERTEX_POINT ( 'NONE', #27680 ) ;
#12185=CARTESIAN_POINT ( 'NONE',  ( -3.766600276044322904, -19.90762401167813067, 11.49999999999999645 ) ) ;
#12187=B_SPLINE_CURVE_WITH_KNOTS ( 'NONE', 3,
 ( #43716, #5147, #36099, #6139, #37092, #67068, #97978, #28476, #68056, #90383, #98979, #62950 ),
 .UNSPECIFIED., .F., .F.,
 ( 4, 2, 2, 2, 2, 4 ),
 ( 0.000000000000000000, 0.0003571373273646645031, 0.0007142746547293290062, 0.001071411982093993564, 0.001249980645776326005, 0.001428549309458658663 ),
 .UNSPECIFIED. ) ;
#12189=CARTESIAN_POINT ( 'NONE',  ( -43.62287095715006302, -23.96177878511307568, 10.65340807706330217 ) ) ;
#12190=VERTEX_POINT ( 'NONE', #49027 ) ;
#12191=CARTESIAN_POINT ( 'NONE',  ( -99.61087926561188510, -25.28548745278821386, 4.301861072295783295 ) ) ;
#12193=DIRECTION ( 'NONE',  ( 0.000000000000000000, -0.9999999999976377785, -2.173523156925979975E-06 ) ) ;
#12195=CARTESIAN_POINT ( 'NONE',  ( -50.67452368755364489, -25.12646064496887988, 7.081740622684785436 ) ) ;
#12196=CARTESIAN_POINT ( 'NONE',  ( 8.743921044546416610, -18.04861246754477477, -1.500000000000002220 ) ) ;
#12197=VECTOR ( 'NONE', #95636, 1000.000000000000227 ) ;
#12199=ORIENTED_EDGE ( 'NONE', *, *, #71885, .T. ) ;
#12201=CARTESIAN_POINT ( 'NONE',  ( -58.62287095715004881, -24.66019654487199020, 8.947790411086131712 ) ) ;
#12202=EDGE_CURVE ( 'NONE', #59550, #64433, #14451, .T. ) ;
#12203=DIRECTION ( 'NONE',  ( -3.773278334453079030E-23, 0.9999999999976377785, 2.173523156925979128E-06 ) ) ;
#12204=CARTESIAN_POINT ( 'NONE',  ( -59.62287095715002749, -23.94994826722514958, -0.6494450866351729745 ) ) ;
#12206=CARTESIAN_POINT ( 'NONE',  ( -105.5228709571500616, -24.99132157543084887, 2.256160258750667502 ) ) ;
#12207=CARTESIAN_POINT ( 'NONE',  ( -89.40841769935767047, -25.12770588385219028, 7.104042889571341668 ) ) ;
#12209=ORIENTED_EDGE ( 'NONE', *, *, #353, .F. ) ;
#12210=CARTESIAN_POINT ( 'NONE',  ( 8.409737122318338365, 18.51778827956368190, -1.500000000000002220 ) ) ;
#12212=B_SPLINE_CURVE_WITH_KNOTS ( 'NONE', 3,
 ( #57868, #89297, #72086, #25895, #87288, #81181 ),
 .UNSPECIFIED., .F., .F.,
 ( 4, 2, 4 ),
 ( 0.000000000000000000, 0.001380764517854761713, 0.002761529035709523426 ),
 .UNSPECIFIED. ) ;
#12213=EDGE_CURVE ( 'NONE', #81670, #78575, #58630, .T. ) ;
#12214=CARTESIAN_POINT ( 'NONE',  ( -22.24355531667433539, 5.575215412481045796, 11.49999999999998934 ) ) ;
#12216=EDGE_LOOP ( 'NONE', ( #76730, #94976, #98601, #86533 ) ) ;
#12217=CARTESIAN_POINT ( 'NONE',  ( -109.5228709571499905, -23.73907113216990084, -1.053371485793244355 ) ) ;
#12218=CARTESIAN_POINT ( 'NONE',  ( -76.52287095715003318, -23.94994826722565406, -0.6494450866342715845 ) ) ;
#12219=CARTESIAN_POINT ( 'NONE',  ( -72.55620429048340725, -23.47593901973091235, -1.443836447539006196 ) ) ;
#12220=CARTESIAN_POINT ( 'NONE',  ( 3.105769797727405024, 20.95935918496786599, 11.49999999999999645 ) ) ;
#12222=CARTESIAN_POINT ( 'NONE',  ( -14.74362065938029076, 16.57599527146691898, 11.49999999999998934 ) ) ;
#12223=CARTESIAN_POINT ( 'NONE',  ( 20.58124611042576646, 0.8182449333618511123, 11.49999999999998934 ) ) ;
#12224=EDGE_LOOP ( 'NONE', ( #62825, #31015, #26636, #83748 ) ) ;
#12225=ORIENTED_EDGE ( 'NONE', *, *, #85862, .T. ) ;
#12226=PLANE ( 'NONE',  #98174 ) ;
#12227=CARTESIAN_POINT ( 'NONE',  ( -49.62287095715004881, -23.72747288104441665, -1.053458166803662444 ) ) ;
#12229=ORIENTED_EDGE ( 'NONE', *, *, #57927, .F. ) ;
#12232=CARTESIAN_POINT ( 'NONE',  ( -28.63639164618194854, -24.19797167907964663, 9.817618374534072601 ) ) ;
#12234=CARTESIAN_POINT ( 'NONE',  ( 16.81283763619640936, 12.23492182941471107, -1.500000000000002220 ) ) ;
#12235=CARTESIAN_POINT ( 'NONE',  ( -21.25272785503416273, -4.502612752106283978, 11.49999999999999645 ) ) ;
#12236=ORIENTED_EDGE ( 'NONE', *, *, #40937, .T. ) ;
#12237=CARTESIAN_POINT ( 'NONE',  ( -113.6228709571500559, -23.48786465467241769, 11.44779295918254114 ) ) ;
#12238=CARTESIAN_POINT ( 'NONE',  ( -115.5528692014212453, -24.52300882791528380, 0.6510814631126371488 ) ) ;
#12239=CARTESIAN_POINT ( 'NONE',  ( -20.38924965233672282, -9.335317855073830273, -1.500000000000002220 ) ) ;
#12241=CARTESIAN_POINT ( 'NONE',  ( -102.5228709571501042, -23.73934037231757443, 11.05740245334328442 ) ) ;
#12243=ORIENTED_EDGE ( 'NONE', *, *, #47366, .T. ) ;
#12245=CARTESIAN_POINT ( 'NONE',  ( -116.4728709571500502, -25.40674640480650126, 5.000950440061918911 ) ) ;
#12246=VERTEX_POINT ( 'NONE', #59633 ) ;
#12247=ORIENTED_EDGE ( 'NONE', *, *, #91233, .T. ) ;
#12248=CARTESIAN_POINT ( 'NONE',  ( -46.48845903137226543, -24.51419770103157347, 9.386484678747180510 ) ) ;
#12249=EDGE_CURVE ( 'NONE', #99250, #32256, #5330, .T. ) ;
#12252=B_SPLINE_CURVE_WITH_KNOTS ( 'NONE', 3,
 ( #68183, #99109, #38717, #8777 ),
 .UNSPECIFIED., .F., .F.,
 ( 4, 4 ),
 ( 0.1606146910193919086, 0.1696211222915076089 ),
 .UNSPECIFIED. ) ;
#12253=CARTESIAN_POINT ( 'NONE',  ( -18.01091527469349529, -11.40912366963296698, -1.500000000000002220 ) ) ;
#12254=ORIENTED_EDGE ( 'NONE', *, *, #56545, .F. ) ;
#12255=CARTESIAN_POINT ( 'NONE',  ( -88.50804541005757642, -24.34968618360933945, 0.1864209137778829184 ) ) ;
#12256=VECTOR ( 'NONE', #6771, 1000.000000000000114 ) ;
#12257=CARTESIAN_POINT ( 'NONE',  ( 21.44370820036873937, 4.193779532373530294, 11.49999999999998934 ) ) ;
#12259=CARTESIAN_POINT ( 'NONE',  ( 22.61316900856233403, 2.020702135111208442, 11.49999999999998934 ) ) ;
#12262=CARTESIAN_POINT ( 'NONE',  ( -81.52287095715006160, -29.50250243563736774, 8.947779886222141599 ) ) ;
#12263=CARTESIAN_POINT ( 'NONE',  ( 19.94191871449930531, -9.063712221575384476, -1.500000000000002220 ) ) ;
#12266=CARTESIAN_POINT ( 'NONE',  ( -122.6250501111026381, -24.15620529776629510, 10.23563542870659582 ) ) ;
#12267=CARTESIAN_POINT ( 'NONE',  ( -40.94687923781921768, -29.50249942614373921, 7.563164501610022405 ) ) ;
#12268=VECTOR ( 'NONE', #99319, 1000.000000000000114 ) ;
#12270=VERTEX_POINT ( 'NONE', #76321 ) ;
#12271=CARTESIAN_POINT ( 'NONE',  ( -41.62287095715006302, -23.48786465467240703, 11.44779295918255180 ) ) ;
#12274=CARTESIAN_POINT ( 'NONE',  ( -0.08811923664316988203, -21.90922723398732330, 0.04347934593173655160 ) ) ;
#12275=CARTESIAN_POINT ( 'NONE',  ( 17.81766572339076404, -11.58780717566545526, -1.500000000000002220 ) ) ;
#12276=CARTESIAN_POINT ( 'NONE',  ( -112.5505015245452540, -24.65952944569305316, 1.056160979905707675 ) ) ;
#12277=CARTESIAN_POINT ( 'NONE',  ( -26.80230302508262241, -24.75186045690199421, 2.622372983264014135 ) ) ;
#12278=EDGE_CURVE ( 'NONE', #29076, #73650, #85623, .T. ) ;
#12279=FACE_OUTER_BOUND ( 'NONE', #1036, .T. ) ;
#12280=CARTESIAN_POINT ( 'NONE',  ( -129.5228709571500758, -23.73907113216990084, -1.053371485793237916 ) ) ;
#12281=EDGE_CURVE ( 'NONE', #33442, #1208, #36027, .T. ) ;
#12282=LINE ( 'NONE', #43258, #19867 ) ;
#12284=CARTESIAN_POINT ( 'NONE',  ( 2.036066721924049805, 19.47704226162102614, 11.49999999999999645 ) ) ;
#12285=DIRECTION ( 'NONE',  ( 0.000000000000000000, -0.9999999999976377785, -2.173523156925979128E-06 ) ) ;
#12286=CARTESIAN_POINT ( 'NONE',  ( -116.5895376238167103, -23.48786465467241769, 11.44779295918253759 ) ) ;
#12287=EDGE_LOOP ( 'NONE', ( #21414, #71161, #94809, #89869 ) ) ;
#12290=CARTESIAN_POINT ( 'NONE',  ( -99.29884676835234814, -25.31439730870533111, 6.107783201820498498 ) ) ;
#12292=CARTESIAN_POINT ( 'NONE',  ( -62.55620429048339304, -23.48783264082478084, -1.443836473390068820 ) ) ;
#12293=CARTESIAN_POINT ( 'NONE',  ( 15.15379598424239838, -12.58889634127381640, 11.49999999999998934 ) ) ;
#12294=B_SPLINE_CURVE_WITH_KNOTS ( 'NONE', 3,
 ( #3580, #96416, #10681, #57381, #27899, #26902, #19773, #10179, #57875, #88812, #19278, #41142, #81189, #35021 ),
 .UNSPECIFIED., .F., .F.,
 ( 4, 2, 2, 2, 2, 2, 4 ),
 ( 8.673617379884035472E-19, 0.0001743298406709247502, 0.0003486596813418486331, 0.0006973193626836755822, 0.001045979044025502694, 0.001220308884696416412, 0.001394638725367330565 ),
 .UNSPECIFIED. ) ;
#12301=CARTESIAN_POINT ( 'NONE',  ( -101.6228709571500559, -24.65952944569304606, 1.056160979905702790 ) ) ;
#12302=CARTESIAN_POINT ( 'NONE',  ( -47.48417913239472909, -24.65952944569304606, 1.056160979905696129 ) ) ;
#12303=CARTESIAN_POINT ( 'NONE',  ( -118.5167440879351375, -24.65952944569305316, 1.056160979905708119 ) ) ;
#12307=CARTESIAN_POINT ( 'NONE',  ( -73.52287095715007581, -24.64898659630528854, 1.056161002820824368 ) ) ;
#12308=CARTESIAN_POINT ( 'NONE',  ( 18.80405327530603543, -6.659971710459020144, 11.49999999999998934 ) ) ;
#12309=EDGE_CURVE ( 'NONE', #12874, #84227, #37293, .T. ) ;
#12311=CARTESIAN_POINT ( 'NONE',  ( -0.06713937605066598591, -22.18082801617931921, 0.4473269341374352392 ) ) ;
#12312=ORIENTED_EDGE ( 'NONE', *, *, #49112, .T. ) ;
#12313=CARTESIAN_POINT ( 'NONE',  ( -128.5895376238167103, -23.48786465467242479, 11.44779295918253403 ) ) ;
#12316=B_SPLINE_CURVE_WITH_KNOTS ( 'NONE', 3,
 ( #96531, #51865, #35144, #66115, #89424, #42764 ),
 .UNSPECIFIED., .F., .F.,
 ( 4, 2, 4 ),
 ( 0.000000000000000000, 0.001380901958385382256, 0.002761803916770764512 ),
 .UNSPECIFIED. ) ;
#12317=DIRECTION ( 'NONE',  ( 1.000000000000000000, 0.000000000000000000, 0.000000000000000000 ) ) ;
#12325=ORIENTED_EDGE ( 'NONE', *, *, #49711, .F. ) ;
#12326=CARTESIAN_POINT ( 'NONE',  ( -64.62287095715008434, -23.96127896941632329, -0.6493128931037873697 ) ) ;
#12327=ADVANCED_FACE ( 'NONE', ( #51518 ), #39284, .T. ) ;
#12329=ORIENTED_EDGE ( 'NONE', *, *, #25961, .F. ) ;
#12331=CARTESIAN_POINT ( 'NONE',  ( 19.68333694646799614, 4.735253856516091098, -1.500000000000002220 ) ) ;
#12332=B_SPLINE_CURVE_WITH_KNOTS ( 'NONE', 3,
 ( #86855, #86365, #16849, #17351, #58433, #34588 ),
 .UNSPECIFIED., .F., .F.,
 ( 4, 2, 4 ),
 ( 0.000000000000000000, 0.001380764517854760629, 0.002761529035709521258 ),
 .UNSPECIFIED. ) ;
#12333=CARTESIAN_POINT ( 'NONE',  ( -122.5921601752248904, -23.48783264082477373, -1.443836473390087471 ) ) ;
#12338=EDGE_CURVE ( 'NONE', #35233, #33585, #80778, .T. ) ;
#12341=CARTESIAN_POINT ( 'NONE',  ( -46.62287095715006302, -23.95044443724992433, 10.65354141964650125 ) ) ;
#12342=CARTESIAN_POINT ( 'NONE',  ( -52.52287095715006870, -23.96177878511308634, 10.65340807706330573 ) ) ;
#12343=CARTESIAN_POINT ( 'NONE',  ( -14.05898297266747221, -14.31596314050798568, -1.500000000000002220 ) ) ;
#12344=CARTESIAN_POINT ( 'NONE',  ( -11.20027426441765961, 17.80179601997297212, 11.49999999999999645 ) ) ;
#12345=DIRECTION ( 'NONE',  ( -3.773278334453080206E-23, 0.9999999999976377785, 2.173523156925979975E-06 ) ) ;
#12346=CARTESIAN_POINT ( 'NONE',  ( -70.53857251337137768, -24.73531770709095312, 8.716586749053510275 ) ) ;
#12347=CARTESIAN_POINT ( 'NONE',  ( -9.261969182712835646, 20.05037652441878038, 11.49999999999998934 ) ) ;
#12348=CARTESIAN_POINT ( 'NONE',  ( -40.41683116089613748, -25.31589329912315378, 5.082404370520299253 ) ) ;
#12350=DIRECTION ( 'NONE',  ( 3.773278334444167608E-23, -1.000000000000000000, 0.000000000000000000 ) ) ;
#12351=ORIENTED_EDGE ( 'NONE', *, *, #42597, .F. ) ;
#12352=CARTESIAN_POINT ( 'NONE',  ( -89.40841769935764205, -25.12049752546738191, 2.832404795212221327 ) ) ;
#12353=CARTESIAN_POINT ( 'NONE',  ( -31.64312605532579425, -24.15543982623907127, -0.2315651400026576545 ) ) ;
#12354=ORIENTED_EDGE ( 'NONE', *, *, #88534, .T. ) ;
#12355=ORIENTED_EDGE ( 'NONE', *, *, #23512, .F. ) ;
#12358=CARTESIAN_POINT ( 'NONE',  ( -76.59623109255625195, -23.96119346886880663, -0.6495511937832059157 ) ) ;
#12359=CARTESIAN_POINT ( 'NONE',  ( 10.54205562766345672, -17.70522803435136083, -1.500000000000002220 ) ) ;
#12360=CARTESIAN_POINT ( 'NONE',  ( 19.98928912078053699, -8.061568661392884749, 11.49999999999999645 ) ) ;
#12363=PLANE ( 'NONE',  #70945 ) ;
#12366=CARTESIAN_POINT ( 'NONE',  ( 7.974090105135403839, 20.87195307945309963, -1.500000000000002220 ) ) ;
#12367=CARTESIAN_POINT ( 'NONE',  ( -59.62287095715002749, -23.96177878511307568, 10.65340807706330573 ) ) ;
#12368=CARTESIAN_POINT ( 'NONE',  ( -65.62287095715005592, -29.50249982740957577, 7.747779886224967605 ) ) ;
#12369=VERTEX_POINT ( 'NONE', #16422 ) ;
#12372=CARTESIAN_POINT ( 'NONE',  ( -7.158894406585330827, 19.61798520005962487, -1.500000000000002220 ) ) ;
#12373=ORIENTED_EDGE ( 'NONE', *, *, #40303, .T. ) ;
#12374=B_SPLINE_CURVE_WITH_KNOTS ( 'NONE', 3,
 ( #14531, #35013, #60732, #73085 ),
 .UNSPECIFIED., .F., .F.,
 ( 4, 4 ),
 ( 0.000000000000000000, 9.999999999998897304E-05 ),
 .UNSPECIFIED. ) ;
#12375=CARTESIAN_POINT ( 'NONE',  ( -86.64361993685139396, -23.48783264082478084, -1.443836473390066155 ) ) ;
#12376=ORIENTED_EDGE ( 'NONE', *, *, #8881, .F. ) ;
#12377=B_SPLINE_CURVE_WITH_KNOTS ( 'NONE', 3,
 ( #65345, #51588, #11025, #82522, #36358, #96263 ),
 .UNSPECIFIED., .F., .F.,
 ( 4, 2, 4 ),
 ( 1.570755371633954459E-05, 0.001396183895866087319, 0.002776660238015835145 ),
 .UNSPECIFIED. ) ;
#12378=ORIENTED_EDGE ( 'NONE', *, *, #18038, .T. ) ;
#12379=ADVANCED_FACE ( 'NONE', ( #39764 ), #78171, .T. ) ;
#12380=CARTESIAN_POINT ( 'NONE',  ( -100.5461013931486605, -24.83644354573578994, 8.397322867130101898 ) ) ;
#12381=CARTESIAN_POINT ( 'NONE',  ( 16.98782256641479904, -12.52229676876588371, -1.500000000000002220 ) ) ;
#12382=ADVANCED_FACE ( 'NONE', ( #92553 ), #52197, .T. ) ;
#12383=ORIENTED_EDGE ( 'NONE', *, *, #34432, .T. ) ;
#12384=CARTESIAN_POINT ( 'NONE',  ( -37.62287095715007013, -23.47596703998600276, 11.44779298504227505 ) ) ;
#12385=CARTESIAN_POINT ( 'NONE',  ( -48.89837313299270960, -25.27432442679760527, 5.876172143706702933 ) ) ;
#12386=CARTESIAN_POINT ( 'NONE',  ( -48.62287095715004881, -23.48786465467241058, 11.44779295918254824 ) ) ;
#12387=CARTESIAN_POINT ( 'NONE',  ( -76.58156790035729955, -24.66019654487199375, 8.947790411086119278 ) ) ;
#12388=CARTESIAN_POINT ( 'NONE',  ( -49.11396232410867668, -25.24991201570810162, 3.837753354500891501 ) ) ;
#12389=CARTESIAN_POINT ( 'NONE',  ( 20.36105213711617878, 7.643125777291208678, -1.500000000000002220 ) ) ;
#12391=CARTESIAN_POINT ( 'NONE',  ( -17.05807961832342912, 14.25954964135033265, 11.49999999999999645 ) ) ;
#12392=ORIENTED_EDGE ( 'NONE', *, *, #28413, .F. ) ;
#12393=CARTESIAN_POINT ( 'NONE',  ( -45.62287095715004170, -24.15431212366391023, -0.2830839119429199857 ) ) ;
#12396=ORIENTED_EDGE ( 'NONE', *, *, #85282, .F. ) ;
#12398=ORIENTED_EDGE ( 'NONE', *, *, #47366, .F. ) ;
#12399=ORIENTED_EDGE ( 'NONE', *, *, #77694, .T. ) ;
#12401=CARTESIAN_POINT ( 'NONE',  ( -49.62287095715005592, -24.65952944569304250, 1.056160979905693020 ) ) ;
#12402=CARTESIAN_POINT ( 'NONE',  ( -49.41588265436393357, -25.31237105244463237, 4.715953302175392103 ) ) ;
#12404=CARTESIAN_POINT ( 'NONE',  ( -87.52287095715006160, -23.47596703998600631, 11.44779298504228393 ) ) ;
#12405=CARTESIAN_POINT ( 'NONE',  ( -121.5228709571500616, -29.50250786944525672, 11.44777988621622811 ) ) ;
#12406=VERTEX_POINT ( 'NONE', #34669 ) ;
#12407=AXIS2_PLACEMENT_3D ( 'NONE', #67300, #91120, #37348 ) ;
#12408=CARTESIAN_POINT ( 'NONE',  ( 16.99290379607386114, -9.356058476803225332, 11.49999999999999645 ) ) ;
#12409=CARTESIAN_POINT ( 'NONE',  ( -115.5228709571501327, -24.92604778743018556, 8.074972756849357225 ) ) ;
#12410=VECTOR ( 'NONE', #2660, 1000.000000000000114 ) ;
#12411=EDGE_CURVE ( 'NONE', #99951, #68864, #27583, .T. ) ;
#12415=EDGE_CURVE ( 'NONE', #71483, #96695, #56725, .T. ) ;
#12419=EDGE_CURVE ( 'NONE', #18110, #62581, #90469, .T. ) ;
#12420=LINE ( 'NONE', #60117, #22847 ) ;
#12421=CARTESIAN_POINT ( 'NONE',  ( 9.507684299284662188, -17.14340340408069707, -1.500000000000002220 ) ) ;
#12422=CARTESIAN_POINT ( 'NONE',  ( -91.15361000704896810, -25.27880950044357178, 5.947789066507965572 ) ) ;
#12424=EDGE_CURVE ( 'NONE', #44696, #36479, #19432, .T. ) ;
#12425=B_SPLINE_CURVE_WITH_KNOTS ( 'NONE', 3,
 ( #2082, #63489, #63995, #78662 ),
 .UNSPECIFIED., .F., .F.,
 ( 4, 4 ),
 ( 0.000000000000000000, 9.999999999998897304E-05 ),
 .UNSPECIFIED. ) ;
#12426=CARTESIAN_POINT ( 'NONE',  ( -19.98823316618875268, 7.996883007359760320, -1.500000000000002220 ) ) ;
#12428=CARTESIAN_POINT ( 'NONE',  ( -80.43221577628075636, -25.30394759211435485, 4.967019781099680564 ) ) ;
#12429=CARTESIAN_POINT ( 'NONE',  ( -50.52287095715006160, -23.84047902841603772, -0.8780736468305390119 ) ) ;
#12430=CARTESIAN_POINT ( 'NONE',  ( -100.1584806888234738, -25.27473227769451114, 3.322325759095222431 ) ) ;
#12431=CARTESIAN_POINT ( 'NONE',  ( 9.898807498884217182, 20.75630955806377287, -1.500000000000002220 ) ) ;
#12433=DIRECTION ( 'NONE',  ( 1.000000000000000000, 3.773278334444167608E-23, 8.201307833595939069E-29 ) ) ;
#12434=CARTESIAN_POINT ( 'NONE',  ( -53.63875608333281519, -24.15543982623906771, -0.2315651400026670359 ) ) ;
#12435=CARTESIAN_POINT ( 'NONE',  ( -19.70923665959843873, 4.302044407003456250, 11.49999999999999645 ) ) ;
#12436=CARTESIAN_POINT ( 'NONE',  ( -109.5317876555421037, -25.28814117369136838, 3.055434580949142553 ) ) ;
#12437=CARTESIAN_POINT ( 'NONE',  ( -32.60153139752230089, -23.96169478059712787, 10.65365249895719124 ) ) ;
#12438=CARTESIAN_POINT ( 'NONE',  ( -46.52287095715006160, -24.65952944569304606, 1.056160979905693686 ) ) ;
#12439=PLANE ( 'NONE',  #55340 ) ;
#12440=CARTESIAN_POINT ( 'NONE',  ( -82.52287095715007581, -23.72773821059537269, 11.05748984161097503 ) ) ;
#12442=CARTESIAN_POINT ( 'NONE',  ( -18.60049703728633474, -6.982253431394513932, 11.49999999999998934 ) ) ;
#12445=CARTESIAN_POINT ( 'NONE',  ( -6.535591236171724105, 18.61618873491671877, -1.500000000000002220 ) ) ;
#12448=CARTESIAN_POINT ( 'NONE',  ( -110.5228709571500616, -24.99156044556120548, 7.747789690856173195 ) ) ;
#12450=CARTESIAN_POINT ( 'NONE',  ( -3.087264924507187924, 20.40197043678811539, 11.49999999999999645 ) ) ;
#12452=CARTESIAN_POINT ( 'NONE',  ( -75.52287095715007581, -23.47596703998600631, 11.44779298504228571 ) ) ;
#12455=CARTESIAN_POINT ( 'NONE',  ( -20.48750165597241590, 9.616757810196778777, 11.49999999999999645 ) ) ;
#12456=B_SPLINE_CURVE_WITH_KNOTS ( 'NONE', 3,
 ( #29236, #13503, #97752, #20128 ),
 .UNSPECIFIED., .F., .F.,
 ( 4, 4 ),
 ( 0.9004288987138345801, 0.9094353299859498918 ),
 .UNSPECIFIED. ) ;
#12457=ORIENTED_EDGE ( 'NONE', *, *, #22244, .T. ) ;
#12459=ADVANCED_FACE ( 'NONE', ( #79828 ), #34171, .T. ) ;
#12461=CARTESIAN_POINT ( 'NONE',  ( -60.52287095715006160, -23.47593901973090169, -1.443836447538996870 ) ) ;
#12462=ADVANCED_FACE ( 'NONE', ( #57520 ), #88456, .T. ) ;
#12464=ORIENTED_EDGE ( 'NONE', *, *, #66279, .F. ) ;
#12467=VERTEX_POINT ( 'NONE', #33157 ) ;
#12469=CARTESIAN_POINT ( 'NONE',  ( 15.09361930729867574, -17.17024899132524496, 11.49999999999998934 ) ) ;
#12470=CARTESIAN_POINT ( 'NONE',  ( -29.61080365403367054, -23.65836453306689080, -1.055554856561816246 ) ) ;
#12472=CARTESIAN_POINT ( 'NONE',  ( 4.073501596442082651, -21.17334570714589859, -1.500000000000002220 ) ) ;
#12473=CARTESIAN_POINT ( 'NONE',  ( -113.5932527405990555, -23.73791477778912196, 11.05961554403170233 ) ) ;
#12474=CARTESIAN_POINT ( 'NONE',  ( -80.48900664166535535, -29.50249842297920466, 7.101626040072651413 ) ) ;
#12475=CARTESIAN_POINT ( 'NONE',  ( 1.861690257272737847, 22.46465895387273903, 11.49999999999999645 ) ) ;
#12476=ORIENTED_EDGE ( 'NONE', *, *, #72802, .T. ) ;
#12477=CARTESIAN_POINT ( 'NONE',  ( -69.75794024142732042, -25.24754266353784260, 4.946031669615599036 ) ) ;
#12478=CARTESIAN_POINT ( 'NONE',  ( 10.07166557822571207, 19.55152498600455857, 11.49999999999998934 ) ) ;
#12481=CARTESIAN_POINT ( 'NONE',  ( -62.62287095715004881, -29.50250243563736774, 8.947779886222145151 ) ) ;
#12485=CARTESIAN_POINT ( 'NONE',  ( -111.6228709571500701, -24.50216790748098461, 0.6166512839513800248 ) ) ;
#12488=DIRECTION ( 'NONE',  ( -3.773278334453079618E-23, 0.9999999999976377785, 2.173523156925979975E-06 ) ) ;
#12489=ORIENTED_EDGE ( 'NONE', *, *, #21802, .T. ) ;
#12491=EDGE_LOOP ( 'NONE', ( #56082, #68905, #493, #34662 ) ) ;
#12492=CARTESIAN_POINT ( 'NONE',  ( -126.5228709571500332, -23.72747288104470442, -1.053458166803224572 ) ) ;
#12494=CARTESIAN_POINT ( 'NONE',  ( -57.49291429130692421, -24.51314013834315375, 0.6176544820404114011 ) ) ;
#12495=CARTESIAN_POINT ( 'NONE',  ( -18.43012528856881715, -8.789534013050598560, -1.500000000000002220 ) ) ;
#12498=CARTESIAN_POINT ( 'NONE',  ( -115.6228709571500701, -24.91570333823100469, 8.075032458375558164 ) ) ;
#12499=CARTESIAN_POINT ( 'NONE',  ( -105.6242956764457972, -24.92564183028979130, 1.928384488918251316 ) ) ;
#12500=CARTESIAN_POINT ( 'NONE',  ( -71.70602904702231228, -25.03149565143765543, 6.253518850926207406 ) ) ;
#12501=VERTEX_POINT ( 'NONE', #44777 ) ;
#12502=CARTESIAN_POINT ( 'NONE',  ( -50.22287095715005734, -23.47596703998600276, 11.44779298504227860 ) ) ;
#12503=CARTESIAN_POINT ( 'NONE',  ( -27.70544111104076990, -24.63646064706438565, 8.251826737477770735 ) ) ;
#12504=ORIENTED_EDGE ( 'NONE', *, *, #59655, .F. ) ;
#12505=CARTESIAN_POINT ( 'NONE',  ( 14.06386034339543478, -15.33156129944631729, -1.500000000000002220 ) ) ;
#12506=EDGE_LOOP ( 'NONE', ( #96885, #89803, #65821, #75291 ) ) ;
#12507=CARTESIAN_POINT ( 'NONE',  ( -40.11295564403756231, -25.30551896248393007, 5.047575478646234792 ) ) ;
#12508=ORIENTED_EDGE ( 'NONE', *, *, #48536, .F. ) ;
#12509=CARTESIAN_POINT ( 'NONE',  ( -28.62287095715004526, -24.34983653798460779, 9.387659975667750345 ) ) ;
#12510=CARTESIAN_POINT ( 'NONE',  ( -123.6228709571500559, -29.50247984919015209, -1.443849546365046699 ) ) ;
#12512=VERTEX_POINT ( 'NONE', #51894 ) ;
#12513=CARTESIAN_POINT ( 'NONE',  ( -114.6228709571500417, -24.65952944569305316, 1.056160979905703234 ) ) ;
#12514=CARTESIAN_POINT ( 'NONE',  ( -64.52287095715006160, -23.48786465467241769, 11.44779295918254824 ) ) ;
#12516=CARTESIAN_POINT ( 'NONE',  ( -71.20303962927951602, -25.31201693143477627, 5.785489938579095437 ) ) ;
#12517=CARTESIAN_POINT ( 'NONE',  ( -5.561696574893697509, -21.35426480686918538, 11.49999999999999645 ) ) ;
#12518=EDGE_LOOP ( 'NONE', ( #70452, #18269, #10542, #39446 ) ) ;
#12519=DIRECTION ( 'NONE',  ( 0.000000000000000000, -0.9999999999976377785, -2.173523156925979128E-06 ) ) ;
#12520=CARTESIAN_POINT ( 'NONE',  ( 16.66146196086182130, -15.28366505690825328, -1.500000000000002220 ) ) ;
#12521=AXIS2_PLACEMENT_3D ( 'NONE', #15007, #20241, #45974 ) ;
#12522=CARTESIAN_POINT ( 'NONE',  ( -115.5168655184217243, -24.40133493613050675, 9.663955038902797057 ) ) ;
#12524=ORIENTED_EDGE ( 'NONE', *, *, #45378, .T. ) ;
#12527=EDGE_CURVE ( 'NONE', #85754, #52727, #22704, .T. ) ;
#12528=CARTESIAN_POINT ( 'NONE',  ( -57.54802801865898232, -24.15620529776628089, 10.23563542870660470 ) ) ;
#12530=CARTESIAN_POINT ( 'NONE',  ( -21.05374637409849825, 2.266213160971460194, 11.49999999999998934 ) ) ;
#12532=CARTESIAN_POINT ( 'NONE',  ( -65.62287095715005592, -23.48783264082478084, -1.443836473390067265 ) ) ;
#12533=CARTESIAN_POINT ( 'NONE',  ( -20.07822104958740539, -9.643837532803976487, -1.500000000000002220 ) ) ;
#12535=EDGE_CURVE ( 'NONE', #10502, #47563, #28846, .T. ) ;
#12536=ORIENTED_EDGE ( 'NONE', *, *, #42355, .F. ) ;
#12538=CARTESIAN_POINT ( 'NONE',  ( -48.62287095715004881, -24.65952944569303895, 1.056160979905692798 ) ) ;
#12539=EDGE_CURVE ( 'NONE', #29076, #92355, #83321, .T. ) ;
#12541=EDGE_CURVE ( 'NONE', #40108, #39879, #73600, .T. ) ;
#12542=CARTESIAN_POINT ( 'NONE',  ( -49.62287095715007013, -23.95044443724992078, 10.65354141964650125 ) ) ;
#12544=CARTESIAN_POINT ( 'NONE',  ( 10.93668938013857783, -16.14717738681254033, -1.500000000000002220 ) ) ;
#12546=CARTESIAN_POINT ( 'NONE',  ( -11.90495014755217618, 17.82271480561356469, -1.500000000000002220 ) ) ;
#12547=CARTESIAN_POINT ( 'NONE',  ( -26.36451126669314604, -24.57999616917673080, 2.180457946598438834 ) ) ;
#12549=DIRECTION ( 'NONE',  ( -3.773278334444167608E-23, 1.000000000000000000, 0.000000000000000000 ) ) ;
#12550=CARTESIAN_POINT ( 'NONE',  ( 0.8422786845129024424, 22.77647355728978340, -1.500000000000002220 ) ) ;
#12554=CARTESIAN_POINT ( 'NONE',  ( -106.5970399906172474, -23.48786465467241769, 11.44779295918253581 ) ) ;
#12556=CARTESIAN_POINT ( 'NONE',  ( 19.57267778704439820, -3.578973306870405047, 11.49999999999999645 ) ) ;
#12557=CARTESIAN_POINT ( 'NONE',  ( -104.5908932905232120, -24.15543982623907482, -0.2315651400026580709 ) ) ;
#12560=CARTESIAN_POINT ( 'NONE',  ( -101.6228709571500559, -24.64898659630368627, 1.056161002820829697 ) ) ;
#12562=CARTESIAN_POINT ( 'NONE',  ( -25.78461022856923890, -24.79966393088477972, 3.119017264803729983 ) ) ;
#12563=EDGE_CURVE ( 'NONE', #45115, #92012, #21410, .T. ) ;
#12564=CARTESIAN_POINT ( 'NONE',  ( -124.5228709571500048, -23.73907113216990084, -1.053371485793245910 ) ) ;
#12565=CARTESIAN_POINT ( 'NONE',  ( -6.179238894844691465, -20.81818906610659425, -1.500000000000002220 ) ) ;
#12566=CARTESIAN_POINT ( 'NONE',  ( -88.88918693012693950, -25.24179881669681080, 6.255794699373288914 ) ) ;
#12567=CARTESIAN_POINT ( 'NONE',  ( -18.23695082634099407, 6.967386181637144738, -1.500000000000002220 ) ) ;
#12569=EDGE_CURVE ( 'NONE', #59330, #45280, #5836, .T. ) ;
#12573=CARTESIAN_POINT ( 'NONE',  ( -20.46784169311667867, 0.4426517378232717737, 11.49999999999999645 ) ) ;
#12575=B_SPLINE_CURVE_WITH_KNOTS ( 'NONE', 3,
 ( #13016, #37374, #98252, #90159, #99253, #42996, #66346, #89662 ),
 .UNSPECIFIED., .F., .F.,
 ( 4, 2, 2, 4 ),
 ( 0.000000000000000000, 0.0005126904249026073470, 0.0007690356373538911796, 0.001025380849805175012 ),
 .UNSPECIFIED. ) ;
#12580=CARTESIAN_POINT ( 'NONE',  ( -75.62287095715005592, -23.47596703998600631, 11.44779298504227860 ) ) ;
#12581=CARTESIAN_POINT ( 'NONE',  ( -99.62287095715005592, -23.47593901973091235, -1.443836447539001089 ) ) ;
#12583=DIRECTION ( 'NONE',  ( 0.000000000000000000, 0.9999999999976377785, 2.173523156925979975E-06 ) ) ;
#12584=AXIS2_PLACEMENT_3D ( 'NONE', #77153, #91386, #21863 ) ;
#12586=CARTESIAN_POINT ( 'NONE',  ( -14.43837761634077310, -17.93274050997184332, 11.49999999999999645 ) ) ;
#12587=CARTESIAN_POINT ( 'NONE',  ( -13.73562189146022661, -18.16285900770654393, 11.49999999999998934 ) ) ;
#12588=CARTESIAN_POINT ( 'NONE',  ( -110.5975890800676780, -23.48786465467241769, 11.44779295918253759 ) ) ;
#12589=B_SPLINE_SURFACE_WITH_KNOTS ( 'NONE', 3, 3, ( 
 ( #74941, #52623, #21161, #83052 ),
 ( #22149, #36397, #90185, #67860 ),
 ( #45024, #44009, #68848, #82567 ),
 ( #75944, #6448, #37405, #29281 ),
 ( #58740, #60252, #29782, #45521 ),
 ( #53137, #83559, #84063, #74460 ),
 ( #68351, #5446, #99766, #37897 ) ),
 .UNSPECIFIED., .F., .F., .F.,
 ( 4, 3, 4 ),
 ( 4, 4 ),
 ( 0.7945040050992232539, 0.8970133687736497885, 0.9995227324480763231 ),
 ( 0.5596362085602246683, 0.5609072983260594558 ),
 .UNSPECIFIED. ) ;
#12592=CARTESIAN_POINT ( 'NONE',  ( -70.52287095715010423, -24.83602698348161297, 1.605859176311264402 ) ) ;
#12593=CARTESIAN_POINT ( 'NONE',  ( -110.6281984393044979, -24.40034930558991633, 0.3402023900116072364 ) ) ;
#12594=ADVANCED_FACE ( 'NONE', ( #13802 ), #62828, .T. ) ;
#12595=CARTESIAN_POINT ( 'NONE',  ( 16.40513048700843513, 14.50174154637248591, 11.49999999999998934 ) ) ;
#12597=CARTESIAN_POINT ( 'NONE',  ( -50.62287095715005592, -23.48786465467241058, 11.44779295918255180 ) ) ;
#12598=CARTESIAN_POINT ( 'NONE',  ( -71.67930401912705918, -25.27253457059604358, 5.900159938492183898 ) ) ;
#12602=CARTESIAN_POINT ( 'NONE',  ( 16.92567061652012228, 11.46397006495115534, 11.49999999999998934 ) ) ;
#12605=ORIENTED_EDGE ( 'NONE', *, *, #96094, .F. ) ;
#12607=CARTESIAN_POINT ( 'NONE',  ( -8.820007276677138464, 21.28423624206370945, -1.500000000000002220 ) ) ;
#12608=CARTESIAN_POINT ( 'NONE',  ( -61.59803820341726777, -23.96119346886880308, -0.6495511937832122440 ) ) ;
#12609=CARTESIAN_POINT ( 'NONE',  ( -5.286950244708777724, -19.55949958832428948, -1.500000000000002220 ) ) ;
#12611=CARTESIAN_POINT ( 'NONE',  ( -69.52287095715006160, -23.47596703998600631, 11.44779298504228748 ) ) ;
#12614=B_SPLINE_CURVE_WITH_KNOTS ( 'NONE', 3,
 ( #53569, #99212, #37826, #61184 ),
 .UNSPECIFIED., .F., .F.,
 ( 4, 4 ),
 ( 0.000000000000000000, 0.0001000000000000028644 ),
 .UNSPECIFIED. ) ;
#12615=B_SPLINE_CURVE_WITH_KNOTS ( 'NONE', 3,
 ( #80216, #90198, #41673, #57405 ),
 .UNSPECIFIED., .F., .F.,
 ( 4, 4 ),
 ( 0.3490140499820214015, 0.3500147970227868166 ),
 .UNSPECIFIED. ) ;
#12616=CARTESIAN_POINT ( 'NONE',  ( -51.62287095715004881, -23.72773821059535138, 11.05748984161097503 ) ) ;
#12617=DIRECTION ( 'NONE',  ( -1.000000000000000000, -3.773278334444166432E-23, -8.201307841325785021E-29 ) ) ;
#12618=CARTESIAN_POINT ( 'NONE',  ( -13.85510387911049079, -16.26762222697724880, 11.49999999999999645 ) ) ;
#12620=FACE_OUTER_BOUND ( 'NONE', #58034, .T. ) ;
#12621=EDGE_LOOP ( 'NONE', ( #15258, #66402, #89594, #21119 ) ) ;
#12622=CARTESIAN_POINT ( 'NONE',  ( 20.56042274393015035, -8.519965759701490171, -1.500000000000002220 ) ) ;
#12623=CARTESIAN_POINT ( 'NONE',  ( -19.40337959798338119, 7.141409694766009508, 11.49999999999998934 ) ) ;
#12625=ORIENTED_EDGE ( 'NONE', *, *, #73195, .T. ) ;
#12626=CARTESIAN_POINT ( 'NONE',  ( -70.78987763377477904, -25.30060019737137367, 6.009288023823078362 ) ) ;
#12627=VERTEX_POINT ( 'NONE', #1605 ) ;
#12628=CARTESIAN_POINT ( 'NONE',  ( -61.58953762381672448, -24.66019654487198665, 8.947790411086129936 ) ) ;
#12630=ORIENTED_EDGE ( 'NONE', *, *, #95022, .F. ) ;
#12631=CARTESIAN_POINT ( 'NONE',  ( 10.03794737889396771, 18.37758748099471973, -1.500000000000002220 ) ) ;
#12632=CARTESIAN_POINT ( 'NONE',  ( -19.17877449816284496, 10.63638241594707345, 11.49999999999999645 ) ) ;
#12633=CARTESIAN_POINT ( 'NONE',  ( -73.64959498640008917, -23.48786465467241058, 11.44779295918254824 ) ) ;
#12634=CARTESIAN_POINT ( 'NONE',  ( -22.39070119279581306, -2.479732019442284496, 11.49999999999998934 ) ) ;
#12635=CARTESIAN_POINT ( 'NONE',  ( 19.40473180639871131, -7.901900427366274293, -1.500000000000002220 ) ) ;
#12636=CARTESIAN_POINT ( 'NONE',  ( -106.5895376238167387, -23.47596703998600631, 11.44779298504227683 ) ) ;
#12637=CARTESIAN_POINT ( 'NONE',  ( -75.52287095715007581, -23.47596703998600631, 11.44779298504228571 ) ) ;
#12638=CARTESIAN_POINT ( 'NONE',  ( -99.52287095715009002, -24.66019654487200441, 8.947790411086119278 ) ) ;
#12640=VERTEX_POINT ( 'NONE', #85830 ) ;
#12641=ORIENTED_EDGE ( 'NONE', *, *, #52203, .T. ) ;
#12642=CARTESIAN_POINT ( 'NONE',  ( -66.58006201227493648, -24.65952944569304250, 1.056160979905692798 ) ) ;
#12643=CARTESIAN_POINT ( 'NONE',  ( -3.867184171070207288, -21.11305558764578194, -1.500000000000002220 ) ) ;
#12645=CARTESIAN_POINT ( 'NONE',  ( -121.6228709571500275, -24.66019654487200441, 8.947790411086119278 ) ) ;
#12647=CARTESIAN_POINT ( 'NONE',  ( -3.607955376466517095, 20.77440192976073519, -1.500000000000002220 ) ) ;
#12649=EDGE_CURVE ( 'NONE', #884, #91131, #45729, .T. ) ;
#12650=CARTESIAN_POINT ( 'NONE',  ( -52.62287095715004170, -24.51283580621364777, 0.6167428607019739273 ) ) ;
#12651=CARTESIAN_POINT ( 'NONE',  ( -50.65952796453198914, -23.85049219812685095, 10.88485053497527133 ) ) ;
#12653=CARTESIAN_POINT ( 'NONE',  ( -129.5219949681614935, -24.15620529776629155, 10.23563542870659759 ) ) ;
#12654=CARTESIAN_POINT ( 'NONE',  ( 7.643743511751816655, -20.74876368896106271, -1.500000000000002220 ) ) ;
#12655=PLANE ( 'NONE',  #15998 ) ;
#12656=ADVANCED_FACE ( 'NONE', ( #31535 ), #15809, .T. ) ;
#12659=EDGE_CURVE ( 'NONE', #65405, #66719, #62632, .T. ) ;
#12660=CARTESIAN_POINT ( 'NONE',  ( -100.6015228439523099, -23.48783264082476663, -1.443836473390090358 ) ) ;
#12662=CARTESIAN_POINT ( 'NONE',  ( 9.194277187580093269, -19.27880637823015419, 11.49999999999998934 ) ) ;
#12663=CARTESIAN_POINT ( 'NONE',  ( -100.6814946224345846, -25.30267106336103922, 4.736250553104468963 ) ) ;
#12664=EDGE_CURVE ( 'NONE', #88647, #71294, #988, .T. ) ;
#12665=CARTESIAN_POINT ( 'NONE',  ( -50.92528559392947329, -25.03707831087709579, 7.590867751134624974 ) ) ;
#12666=CARTESIAN_POINT ( 'NONE',  ( -0.1469176100155287212, -21.14803608454491268, 11.46586199002818951 ) ) ;
#12668=CARTESIAN_POINT ( 'NONE',  ( -22.43363504178351775, 2.973318333978472339, -1.500000000000002220 ) ) ;
#12669=B_SPLINE_SURFACE_WITH_KNOTS ( 'NONE', 3, 3, ( 
 ( #31476, #23854, #23344, #46712 ),
 ( #60938, #62436, #7641, #76137 ),
 ( #93363, #6634, #54829, #38587 ),
 ( #54329, #53826, #70037, #85764 ),
 ( #22340, #83754, #62947, #24363 ),
 ( #37590, #30970, #53324, #84254 ),
 ( #14739, #15245, #85254, #7132 ) ),
 .UNSPECIFIED., .F., .F., .F.,
 ( 4, 3, 4 ),
 ( 4, 4 ),
 ( 0.7945040050992242531, 0.8970133687736501216, 0.9995227324480759901 ),
 ( 0.5196260414224536106, 0.5208786598400961809 ),
 .UNSPECIFIED. ) ;
#12670=ORIENTED_EDGE ( 'NONE', *, *, #68543, .T. ) ;
#12672=CARTESIAN_POINT ( 'NONE',  ( -79.54044106604338538, -24.65952944569304606, 1.056160979905700126 ) ) ;
#12673=CARTESIAN_POINT ( 'NONE',  ( 3.912202881759007767, 19.34271161525698091, 11.49999999999999645 ) ) ;
#12678=CARTESIAN_POINT ( 'NONE',  ( -29.12854162637831834, -24.60094034115323680, 2.289900629743222282 ) ) ;
#12680=CARTESIAN_POINT ( 'NONE',  ( 5.568959250215116619, -20.88136358707659923, -1.500000000000002220 ) ) ;
#12683=CARTESIAN_POINT ( 'NONE',  ( -12.28997142660015740, 14.97987746540053422, -1.500000000000002220 ) ) ;
#12684=CARTESIAN_POINT ( 'NONE',  ( -50.52287095715006160, -23.47593901973090169, -1.443836447538997092 ) ) ;
#12685=CARTESIAN_POINT ( 'NONE',  ( -81.38737579674543099, -25.10497842348888042, 7.257320789189920518 ) ) ;
#12686=CARTESIAN_POINT ( 'NONE',  ( -18.99895575154661742, -5.639348582513488140, 11.49999999999998934 ) ) ;
#12687=VERTEX_POINT ( 'NONE', #23922 ) ;
#12688=CARTESIAN_POINT ( 'NONE',  ( 19.26017855675105750, 6.235128648364509196, 11.49999999999999645 ) ) ;
#12689=FACE_OUTER_BOUND ( 'NONE', #67223, .T. ) ;
#12690=CARTESIAN_POINT ( 'NONE',  ( -51.62287095715005592, -24.65952944569304250, 1.056160979905695019 ) ) ;
#12691=ORIENTED_EDGE ( 'NONE', *, *, #77301, .T. ) ;
#12695=CARTESIAN_POINT ( 'NONE',  ( -92.52287095715009002, -24.66019654487200086, 8.947790411086115725 ) ) ;
#12696=CARTESIAN_POINT ( 'NONE',  ( -60.52287095715006160, -29.50249982740957577, 7.747779886224967605 ) ) ;
#12697=CARTESIAN_POINT ( 'NONE',  ( -12.65591448191638335, 15.52279176289047236, 11.49999999999998934 ) ) ;
#12699=ORIENTED_EDGE ( 'NONE', *, *, #12281, .F. ) ;
#12700=AXIS2_PLACEMENT_3D ( 'NONE', #94568, #63644, #38779 ) ;
#12701=CARTESIAN_POINT ( 'NONE',  ( -49.50986403386431078, -25.31297060778654995, 4.014908341799525715 ) ) ;
#12703=CARTESIAN_POINT ( 'NONE',  ( -129.5228709571500758, -24.64965694238408034, 8.947790433994189385 ) ) ;
#12706=CARTESIAN_POINT ( 'NONE',  ( -79.11611000704996854, -29.50248939449842922, 2.947779886236309377 ) ) ;
#12709=VERTEX_POINT ( 'NONE', #93428 ) ;
#12710=CARTESIAN_POINT ( 'NONE',  ( 3.964343641299885146, 19.94596313931659992, 11.49999999999998934 ) ) ;
#12711=EDGE_LOOP ( 'NONE', ( #93864, #25530, #27483, #91794 ) ) ;
#12712=CARTESIAN_POINT ( 'NONE',  ( 20.74614131242519477, 9.816050768296040729, 11.49999999999998934 ) ) ;
#12715=CARTESIAN_POINT ( 'NONE',  ( -89.52287095715003318, -23.48783264083374789, -1.443836473376144180 ) ) ;
#12716=CARTESIAN_POINT ( 'NONE',  ( -49.27993637813898431, -25.12215232176118107, 6.239169103029740704 ) ) ;
#12717=CARTESIAN_POINT ( 'NONE',  ( -38.55620429048340725, -24.66019654487199020, 8.947790411086135265 ) ) ;
#12718=CARTESIAN_POINT ( 'NONE',  ( -14.68016216564755894, -15.32010671487267572, 11.49999999999999645 ) ) ;
#12719=ORIENTED_EDGE ( 'NONE', *, *, #17382, .F. ) ;
#12721=CARTESIAN_POINT ( 'NONE',  ( -20.56242917251232782, -8.299981740788712870, -1.500000000000002220 ) ) ;
#12722=CARTESIAN_POINT ( 'NONE',  ( 1.511266892140219920, 20.53031905857337591, -1.500000000000002220 ) ) ;
#12724=ORIENTED_EDGE ( 'NONE', *, *, #22814, .F. ) ;
#12725=DIRECTION ( 'NONE',  ( -1.000000000000000000, -3.773278334444167608E-23, -8.201307833595939069E-29 ) ) ;
#12726=CARTESIAN_POINT ( 'NONE',  ( -49.62287095715004881, -24.50216790748097395, 0.6166512839513585975 ) ) ;
#12728=VERTEX_POINT ( 'NONE', #70606 ) ;
#12730=VERTEX_POINT ( 'NONE', #589 ) ;
#12732=CARTESIAN_POINT ( 'NONE',  ( -71.52287095715007581, -24.64965694238408034, 8.947790433994200043 ) ) ;
#12734=CARTESIAN_POINT ( 'NONE',  ( -18.43438512255917772, -9.567967903218889347, -1.500000000000002220 ) ) ;
#12735=CARTESIAN_POINT ( 'NONE',  ( 17.47290450027814757, -12.96279059203284767, 11.49999999999999645 ) ) ;
#12736=ORIENTED_EDGE ( 'NONE', *, *, #37346, .F. ) ;
#12737=CARTESIAN_POINT ( 'NONE',  ( -44.62287095715004881, -29.50248528299804818, 1.056150453629031594 ) ) ;
#12738=CARTESIAN_POINT ( 'NONE',  ( -98.89303308397303738, -25.25494757631710385, 6.110950176066591411 ) ) ;
#12740=CARTESIAN_POINT ( 'NONE',  ( -21.67104271438225638, 5.786422744429515319, -1.500000000000002220 ) ) ;
#12743=CARTESIAN_POINT ( 'NONE',  ( -65.55949795840675165, -23.85016227208580730, -0.8807180028928343063 ) ) ;
#12745=CARTESIAN_POINT ( 'NONE',  ( -75.52287095715007581, -23.47593901973090169, -1.443836447538996870 ) ) ;
#12749=EDGE_LOOP ( 'NONE', ( #15637, #66835, #35684, #19356 ) ) ;
#12751=ORIENTED_EDGE ( 'NONE', *, *, #13158, .F. ) ;
#12752=B_SPLINE_CURVE_WITH_KNOTS ( 'NONE', 3,
 ( #55587, #71304, #56593, #73791, #90020, #4290, #35240, #44355, #42862, #11397, #12385, #75280, #51962, #27125 ),
 .UNSPECIFIED., .F., .F.,
 ( 4, 2, 2, 2, 2, 2, 4 ),
 ( 9.813077866773594792E-18, 0.0001940785162856977137, 0.0003881570325713856154, 0.0007763140651427799044, 0.001164471097714174031, 0.001358549613999873208, 0.001552628130285572602 ),
 .UNSPECIFIED. ) ;
#12753=CARTESIAN_POINT ( 'NONE',  ( -8.014198274750887308, -19.69740135394370384, -1.500000000000002220 ) ) ;
#12756=CARTESIAN_POINT ( 'NONE',  ( 17.39636294008568740, -13.23181597624684791, -1.500000000000002220 ) ) ;
#12757=CARTESIAN_POINT ( 'NONE',  ( -124.5895376238167387, -23.47596703998600631, 11.44779298504227683 ) ) ;
#12758=CARTESIAN_POINT ( 'NONE',  ( 4.020035926878589905, 22.33396232419688587, -1.500000000000002220 ) ) ;
#12759=AXIS2_PLACEMENT_3D ( 'NONE', #78466, #86091, #94703 ) ;
#12762=CARTESIAN_POINT ( 'NONE',  ( 20.73430856240977249, 7.200853762728330665, -1.500000000000002220 ) ) ;
#12763=CARTESIAN_POINT ( 'NONE',  ( -100.5228709571500616, -25.00158670708909625, 2.256160236439166411 ) ) ;
#12765=CARTESIAN_POINT ( 'NONE',  ( -122.5572053947523585, -23.48786465467241769, 11.44779295918253581 ) ) ;
#12768=ADVANCED_FACE ( 'NONE', ( #63013 ), #86330, .T. ) ;
#12770=DIRECTION ( 'NONE',  ( 3.773278334444167608E-23, -1.000000000000000000, 0.000000000000000000 ) ) ;
#12771=EDGE_CURVE ( 'NONE', #833, #52813, #13012, .T. ) ;
#12773=CARTESIAN_POINT ( 'NONE',  ( -0.05753151201984656182, -22.30520936630598072, 1.095224832288506089 ) ) ;
#12774=CARTESIAN_POINT ( 'NONE',  ( -20.86817740539179056, 4.147639786170328691, -1.500000000000002220 ) ) ;
#12776=EDGE_CURVE ( 'NONE', #61188, #10237, #72340, .T. ) ;
#12777=CARTESIAN_POINT ( 'NONE',  ( -26.10669942825130363, -24.97064885537375645, 4.499505497235293916 ) ) ;
#12778=CARTESIAN_POINT ( 'NONE',  ( -85.59145065735712876, -24.40034930558991633, 0.3402023900116044608 ) ) ;
#12779=CARTESIAN_POINT ( 'NONE',  ( -68.55932668679069764, -23.73766607897670156, -1.055555164236458232 ) ) ;
#12781=CARTESIAN_POINT ( 'NONE',  ( -32.58953762381671737, -23.47593901973091235, -1.443836447539013301 ) ) ;
#12783=CARTESIAN_POINT ( 'NONE',  ( -9.112395119859147741, -17.30902560603237106, 11.49999999999999645 ) ) ;
#12784=CARTESIAN_POINT ( 'NONE',  ( -78.52287095715006160, -24.35013146730203815, 9.818937971375097717 ) ) ;
#12785=CARTESIAN_POINT ( 'NONE',  ( -118.5228709571501184, -23.48783264082477373, -1.443836473390083475 ) ) ;
#12786=EDGE_CURVE ( 'NONE', #29980, #9998, #9710, .T. ) ;
#12788=DIRECTION ( 'NONE',  ( -3.773278334453079030E-23, 0.9999999999976377785, 2.173523156925979128E-06 ) ) ;
#12790=CARTESIAN_POINT ( 'NONE',  ( -27.24607494285254816, -24.62946685170201633, 8.199799071658667060 ) ) ;
#12791=CARTESIAN_POINT ( 'NONE',  ( -75.52287095715004739, -25.00182538069145366, 7.747789668545101094 ) ) ;
#12792=CARTESIAN_POINT ( 'NONE',  ( 10.64064036176630879, -16.58286410872727146, -1.500000000000002220 ) ) ;
#12794=CARTESIAN_POINT ( 'NONE',  ( -108.6228709571500417, -23.47596703998600631, 11.44779298504227860 ) ) ;
#12799=LINE ( 'NONE', #84314, #86318 ) ;
#12800=CARTESIAN_POINT ( 'NONE',  ( -47.66149957754198851, -23.48783264082478084, -1.443836473390071928 ) ) ;
#12801=CARTESIAN_POINT ( 'NONE',  ( -118.5902651629808560, -24.15543982623907837, -0.2315651400026558782 ) ) ;
#12802=PLANE ( 'NONE',  #9605 ) ;
#12806=CARTESIAN_POINT ( 'NONE',  ( -85.55620429048337883, -25.00158670708909625, 2.256160236439166855 ) ) ;
#12807=CARTESIAN_POINT ( 'NONE',  ( 18.73470368118781693, 6.836574088118649861, 11.49999999999998934 ) ) ;
#12809=CARTESIAN_POINT ( 'NONE',  ( -0.008299077606883394423, -22.94256191861778760, 3.420120028211836694 ) ) ;
#12811=VECTOR ( 'NONE', #32571, 1000.000000000000114 ) ;
#12814=EDGE_CURVE ( 'NONE', #39855, #733, #33693, .T. ) ;
#12817=CARTESIAN_POINT ( 'NONE',  ( -127.4728709572981415, -25.30561157749831480, 5.197923170786341807 ) ) ;
#12818=CARTESIAN_POINT ( 'NONE',  ( -81.55065612788921214, -24.15543982623907482, -0.2315651400026469686 ) ) ;
#12821=CARTESIAN_POINT ( 'NONE',  ( -75.52287095715007581, -23.47593901973090169, -1.443836447538996870 ) ) ;
#12822=CARTESIAN_POINT ( 'NONE',  ( -51.09576285965076181, -25.26280100839387543, 4.912419055384075861 ) ) ;
#12823=ORIENTED_EDGE ( 'NONE', *, *, #99672, .F. ) ;
#12824=CARTESIAN_POINT ( 'NONE',  ( -34.62287095715005592, -24.65952944569303895, 1.056160979905691688 ) ) ;
#12825=CARTESIAN_POINT ( 'NONE',  ( -127.5219661461652265, -23.73766607897670866, -1.055555164236447574 ) ) ;
#12826=ORIENTED_EDGE ( 'NONE', *, *, #62083, .F. ) ;
#12827=VECTOR ( 'NONE', #25207, 1000.000000000000114 ) ;
#12828=B_SPLINE_CURVE_WITH_KNOTS ( 'NONE', 3,
 ( #96967, #12217, #36064, #50306, #90353, #34581 ),
 .UNSPECIFIED., .F., .F.,
 ( 4, 2, 4 ),
 ( 6.384118678616914202E-06, 0.001386860460828380189, 0.002767336802978143193 ),
 .UNSPECIFIED. ) ;
#12829=CARTESIAN_POINT ( 'NONE',  ( 12.15850541088210868, 16.18036119754114566, -1.500000000000002220 ) ) ;
#12830=CARTESIAN_POINT ( 'NONE',  ( -128.5228709571501042, -24.66019654487200441, 8.947790411086108620 ) ) ;
#12832=CARTESIAN_POINT ( 'NONE',  ( -86.52287095715006160, -29.50247984919015209, -1.443849546365051806 ) ) ;
#12833=EDGE_LOOP ( 'NONE', ( #45067, #13051, #8692, #19143, #50817, #48485, #92645, #12947, #74760, #45977, #18158, #91579 ) ) ;
#12834=CARTESIAN_POINT ( 'NONE',  ( -77.52287095715006160, -24.33927499327854349, 9.819080762295806508 ) ) ;
#12836=CARTESIAN_POINT ( 'NONE',  ( -19.96166555454951208, -2.086822695551191043, -1.500000000000002220 ) ) ;
#12837=CARTESIAN_POINT ( 'NONE',  ( 17.94697546605861760, -10.91086909363634838, 11.49999999999999645 ) ) ;
#12838=CARTESIAN_POINT ( 'NONE',  ( -27.83177597161019179, -24.82260152899532102, 7.598324359836099440 ) ) ;
#12839=CARTESIAN_POINT ( 'NONE',  ( -32.52287095715005449, -23.73907113217656573, -1.053371485781500860 ) ) ;
#12840=CARTESIAN_POINT ( 'NONE',  ( -21.77411086464670831, -3.637377321037103872, -1.500000000000002220 ) ) ;
#12843=VECTOR ( 'NONE', #87953, 1000.000000000000114 ) ;
#12844=CARTESIAN_POINT ( 'NONE',  ( -76.58953762381673869, -23.47593901973091235, -1.443836447539004642 ) ) ;
#12845=FACE_OUTER_BOUND ( 'NONE', #84777, .T. ) ;
#12848=B_SPLINE_SURFACE_WITH_KNOTS ( 'NONE', 3, 3, ( 
 ( #73766, #66688, #43822, #29582 ),
 ( #68157, #66187, #12854, #97107 ),
 ( #59553, #12358, #51438, #19974 ),
 ( #74269, #35714, #74756, #37204 ),
 ( #5252, #21456, #51937, #82866 ),
 ( #67669, #44329, #75258, #5750 ),
 ( #98590, #13853, #29084, #60058 ) ),
 .UNSPECIFIED., .F., .F., .F.,
 ( 4, 3, 4 ),
 ( 4, 4 ),
 ( 0.0004766839783822049946, 0.1029713700210897892, 0.2054660560637973643 ),
 ( 0.5396312702239698389, 0.5408929796565489223 ),
 .UNSPECIFIED. ) ;
#12849=LINE ( 'NONE', #81876, #9717 ) ;
#12851=ORIENTED_EDGE ( 'NONE', *, *, #86227, .F. ) ;
#12852=CARTESIAN_POINT ( 'NONE',  ( -55.52287095715008292, -24.52232992886361629, 0.6492154411906015943 ) ) ;
#12853=CARTESIAN_POINT ( 'NONE',  ( -97.52287095715006160, -24.65952944569304606, 1.056160979905702346 ) ) ;
#12854=CARTESIAN_POINT ( 'NONE',  ( -76.55889680453810797, -23.73766607897670866, -1.055555164236452681 ) ) ;
#12855=CARTESIAN_POINT ( 'NONE',  ( -10.57813111170615983, 17.65445453266677234, -1.500000000000002220 ) ) ;
#12856=CARTESIAN_POINT ( 'NONE',  ( -20.03152041342270806, -8.007337437543776915, 11.49999999999999645 ) ) ;
#12859=CARTESIAN_POINT ( 'NONE',  ( -121.6228709571500417, -23.48786465467241769, 11.44779295918253759 ) ) ;
#12861=CARTESIAN_POINT ( 'NONE',  ( 13.15158565771796084, -18.08388448789661851, -1.500000000000002220 ) ) ;
#12862=CARTESIAN_POINT ( 'NONE',  ( -62.52287095715006160, -23.48783264082477018, -1.443836473390091912 ) ) ;
#12863=CARTESIAN_POINT ( 'NONE',  ( -84.63607199451277552, -23.96119346886880663, -0.6495511937832096905 ) ) ;
#12865=PLANE ( 'NONE',  #24189 ) ;
#12866=PLANE ( 'NONE',  #68566 ) ;
#12867=CARTESIAN_POINT ( 'NONE',  ( -0.8937202392249329330, 20.86669477224961256, -1.500000000000002220 ) ) ;
#12872=CARTESIAN_POINT ( 'NONE',  ( -100.5179223032556024, -23.85049219812686161, 10.88485053497527133 ) ) ;
#12873=CARTESIAN_POINT ( 'NONE',  ( -16.61111445048470614, -13.04167290785011701, -1.500000000000002220 ) ) ;
#12874=VERTEX_POINT ( 'NONE', #25431 ) ;
#12875=CARTESIAN_POINT ( 'NONE',  ( -117.5885033326503475, -24.51314013834316086, 0.6176544820404201719 ) ) ;
#12877=CARTESIAN_POINT ( 'NONE',  ( -109.8650282762807393, -25.28040082146351608, 5.784628005357986602 ) ) ;
#12878=VECTOR ( 'NONE', #89621, 1000.000000000000114 ) ;
#12879=DIRECTION ( 'NONE',  ( 0.000000000000000000, -2.173523156925979552E-06, 0.9999999999976378895 ) ) ;
#12880=CARTESIAN_POINT ( 'NONE',  ( -49.10457154551148307, -25.26416398485831749, 3.999772271414141489 ) ) ;
#12881=CARTESIAN_POINT ( 'NONE',  ( -11.39883337241029793, 18.50525654427185884, -1.500000000000002220 ) ) ;
#12882=CARTESIAN_POINT ( 'NONE',  ( -107.5562042904834072, -23.48783264082478794, -1.443836473390060160 ) ) ;
#12884=CARTESIAN_POINT ( 'NONE',  ( 20.80681148587913754, 8.022540738981085440, 11.49999999999999645 ) ) ;
#12886=CARTESIAN_POINT ( 'NONE',  ( -129.6228709571500417, -24.65952944569305316, 1.056160979905706121 ) ) ;
#12888=CARTESIAN_POINT ( 'NONE',  ( -106.5228709571500616, -24.50321055353805733, 9.387540953477520489 ) ) ;
#12889=ORIENTED_EDGE ( 'NONE', *, *, #17141, .F. ) ;
#12890=ORIENTED_EDGE ( 'NONE', *, *, #94958, .T. ) ;
#12892=ORIENTED_EDGE ( 'NONE', *, *, #17584, .T. ) ;
#12893=EDGE_CURVE ( 'NONE', #77615, #91001, #67488, .T. ) ;
#12897=EDGE_CURVE ( 'NONE', #53473, #45924, #44482, .T. ) ;
#12898=CARTESIAN_POINT ( 'NONE',  ( -52.55620429048340014, -23.48786465467241058, 11.44779295918254647 ) ) ;
#12903=EDGE_LOOP ( 'NONE', ( #32750, #75800, #38221, #82288 ) ) ;
#12905=CARTESIAN_POINT ( 'NONE',  ( 7.147005326088517130, -18.03964237587283037, 11.49999999999999645 ) ) ;
#12907=CARTESIAN_POINT ( 'NONE',  ( -130.5728709571500303, -23.86862559985391741, 11.02355999656199792 ) ) ;
#12909=ORIENTED_EDGE ( 'NONE', *, *, #20908, .T. ) ;
#12913=CARTESIAN_POINT ( 'NONE',  ( -120.6228709571500417, -23.47596703998600631, 11.44779298504227683 ) ) ;
#12914=CARTESIAN_POINT ( 'NONE',  ( 18.62133539762988121, 6.091496293051981148, 11.49999999999998934 ) ) ;
#12916=ORIENTED_EDGE ( 'NONE', *, *, #13517, .F. ) ;
#12917=CARTESIAN_POINT ( 'NONE',  ( -8.857468890034409625, -19.66367526556523870, 11.49999999999998934 ) ) ;
#12918=FACE_OUTER_BOUND ( 'NONE', #77671, .T. ) ;
#12920=CARTESIAN_POINT ( 'NONE',  ( -40.65336132159010418, -24.15503026093912453, -0.2815557561904605266 ) ) ;
#12921=DIRECTION ( 'NONE',  ( -3.773278334453079030E-23, 0.9999999999976377785, 2.173523156925979128E-06 ) ) ;
#12922=CARTESIAN_POINT ( 'NONE',  ( 14.37299948674089123, 17.95305339730678185, -1.500000000000002220 ) ) ;
#12923=B_SPLINE_CURVE_WITH_KNOTS ( 'NONE', 3,
 ( #482, #8605, #31436, #54789, #47173, #72014, #73010, #2495, #57299, #26820, #81106, #57785, #81610, #65417, #35441, #50662 ),
 .UNSPECIFIED., .F., .F.,
 ( 4, 2, 2, 2, 2, 2, 2, 4 ),
 ( 2.195984522899320023E-17, 0.0002681372138471760217, 0.0005362744276943301426, 0.001072548855388625374, 0.001340686069235787247, 0.001608823283082948686, 0.001876960496930110342, 0.002145097710777272432 ),
 .UNSPECIFIED. ) ;
#12926=DIRECTION ( 'NONE',  ( -3.773278334453079618E-23, 0.9999999999976377785, 2.173523156925979975E-06 ) ) ;
#12927=CARTESIAN_POINT ( 'NONE',  ( -17.16780662754360520, -10.58209718439171176, 11.49999999999999645 ) ) ;
#12928=CARTESIAN_POINT ( 'NONE',  ( -109.0059884841570153, -25.28814275788919019, 3.784296300591792228 ) ) ;
#12932=B_SPLINE_CURVE_WITH_KNOTS ( 'NONE', 3,
 ( #96571, #49928, #27072, #12326, #61017, #75227 ),
 .UNSPECIFIED., .F., .F.,
 ( 4, 2, 4 ),
 ( 1.570755371634052715E-05, 0.001396183895866089488, 0.002776660238015838181 ),
 .UNSPECIFIED. ) ;
#12933=CARTESIAN_POINT ( 'NONE',  ( -38.52287095715006870, -24.64898659630367206, 1.056161002820819261 ) ) ;
#12935=CARTESIAN_POINT ( 'NONE',  ( -5.703961651189128901, -19.02375728206049743, -1.500000000000002220 ) ) ;
#12936=FACE_OUTER_BOUND ( 'NONE', #67833, .T. ) ;
#12937=CARTESIAN_POINT ( 'NONE',  ( 16.04393857186779115, -11.51807295290239885, -1.500000000000002220 ) ) ;
#12938=CARTESIAN_POINT ( 'NONE',  ( -126.6245546122516714, -23.96169478059714564, 10.65365249895716637 ) ) ;
#12939=CARTESIAN_POINT ( 'NONE',  ( -125.6228709571500843, -24.51254535404253687, 9.355368623467642308 ) ) ;
#12941=CARTESIAN_POINT ( 'NONE',  ( 20.35908867758196550, 3.722869731652943770, 11.49999999999999645 ) ) ;
#12942=CARTESIAN_POINT ( 'NONE',  ( -53.62287095715005592, -24.66019654487199375, 8.947790411086135265 ) ) ;
#12945=CARTESIAN_POINT ( 'NONE',  ( 18.27610663105864219, 13.37729726205769154, 11.49999999999999645 ) ) ;
#12946=EDGE_CURVE ( 'NONE', #41731, #18934, #52914, .T. ) ;
#12947=ORIENTED_EDGE ( 'NONE', *, *, #61263, .T. ) ;
#12950=AXIS2_PLACEMENT_3D ( 'NONE', #42718, #28462, #5132 ) ;
#12951=CARTESIAN_POINT ( 'NONE',  ( -63.50465895583770504, -24.15543982623906416, -0.2315651400026651485 ) ) ;
#12957=CARTESIAN_POINT ( 'NONE',  ( -21.74799678179195794, 7.114197580472080951, -1.500000000000002220 ) ) ;
#12958=CARTESIAN_POINT ( 'NONE',  ( -29.63600644203553003, -24.27415457529449938, 0.1864212292069159782 ) ) ;
#12960=CARTESIAN_POINT ( 'NONE',  ( 10.40854797073303395, 18.91789161722374146, -1.500000000000002220 ) ) ;
#12961=FACE_OUTER_BOUND ( 'NONE', #77280, .T. ) ;
#12963=CARTESIAN_POINT ( 'NONE',  ( -3.310667818835141940, 22.29536907041311977, 11.49999999999999645 ) ) ;
#12964=ORIENTED_EDGE ( 'NONE', *, *, #16778, .F. ) ;
#12965=AXIS2_PLACEMENT_3D ( 'NONE', #60295, #75483, #31694 ) ;
#12966=CARTESIAN_POINT ( 'NONE',  ( -27.68651082257922980, -24.78174777341091328, 2.274903344755643708 ) ) ;
#12967=CARTESIAN_POINT ( 'NONE',  ( 8.537626919312410578, 20.26776412955123163, -1.500000000000002220 ) ) ;
#12970=CARTESIAN_POINT ( 'NONE',  ( -111.5936661300013952, -23.73766607897671221, -1.055555164236450905 ) ) ;
#12971=CARTESIAN_POINT ( 'NONE',  ( -41.86995616089613748, -25.10926067824552632, 4.210710108100564675 ) ) ;
#12973=DIRECTION ( 'NONE',  ( 3.773278334444166432E-23, -1.000000000000000000, 0.000000000000000000 ) ) ;
#12974=CARTESIAN_POINT ( 'NONE',  ( -90.50426386717819582, -24.63419186844611275, 9.035850630976923981 ) ) ;
#12977=ADVANCED_FACE ( 'NONE', ( #48792 ), #34055, .F. ) ;
#12980=CARTESIAN_POINT ( 'NONE',  ( -65.52287095715011844, -24.62226745350437795, 0.9660975649728075210 ) ) ;
#12981=CARTESIAN_POINT ( 'NONE',  ( -72.22287095715007865, -23.47596703998600631, 11.44779298504227860 ) ) ;
#12982=CARTESIAN_POINT ( 'NONE',  ( -36.61836639171551866, -23.48783264082477018, -1.443836473390095909 ) ) ;
#12983=CARTESIAN_POINT ( 'NONE',  ( -0.5597704280004801580, 20.37679164443051505, -1.500000000000002220 ) ) ;
#12984=EDGE_LOOP ( 'NONE', ( #35258, #46087, #23060, #90654 ) ) ;
#12986=EDGE_CURVE ( 'NONE', #73782, #13191, #84465, .T. ) ;
#12987=CARTESIAN_POINT ( 'NONE',  ( -69.52287095715003318, -24.66019654487199375, 8.947790411086119278 ) ) ;
#12990=DIRECTION ( 'NONE',  ( -1.000000000000000000, -3.773278334444167608E-23, -8.201307833595939069E-29 ) ) ;
#12991=ORIENTED_EDGE ( 'NONE', *, *, #91233, .F. ) ;
#12993=CARTESIAN_POINT ( 'NONE',  ( -40.41683116089613748, -25.30532407203700984, 5.082404393492757855 ) ) ;
#12994=EDGE_CURVE ( 'NONE', #75736, #43450, #56643, .T. ) ;
#12995=CARTESIAN_POINT ( 'NONE',  ( 20.50115541507891948, 3.495740877612329101, 11.49999999999998934 ) ) ;
#12996=ORIENTED_EDGE ( 'NONE', *, *, #80716, .T. ) ;
#12997=DIRECTION ( 'NONE',  ( 3.773278334444167608E-23, -1.000000000000000000, 0.000000000000000000 ) ) ;
#12999=CARTESIAN_POINT ( 'NONE',  ( -44.62287095715004881, -23.47596703998600631, 11.44779298504227505 ) ) ;
#13000=CARTESIAN_POINT ( 'NONE',  ( -33.52287095715008292, -24.33832256527048088, 0.1851278514138557096 ) ) ;
#13001=ORIENTED_EDGE ( 'NONE', *, *, #88327, .F. ) ;
#13003=CARTESIAN_POINT ( 'NONE',  ( -112.5228709571500616, -23.48783264083431988, -1.443836473375253782 ) ) ;
#13005=CARTESIAN_POINT ( 'NONE',  ( -35.62287095715005592, -29.50247984919015209, -1.443849546365060466 ) ) ;
#13006=CARTESIAN_POINT ( 'NONE',  ( -71.04293837957820301, -25.24515098662989487, 5.573254966138859068 ) ) ;
#13008=CARTESIAN_POINT ( 'NONE',  ( -5.973063517705734071, 21.31661749205449041, 11.49999999999999645 ) ) ;
#13010=CARTESIAN_POINT ( 'NONE',  ( -108.5222109390871594, -23.48783264082478084, -1.443836473390062602 ) ) ;
#13011=CARTESIAN_POINT ( 'NONE',  ( -13.31036990564671818, -18.29084955798148471, 11.49999999999998934 ) ) ;
#13012=B_SPLINE_CURVE_WITH_KNOTS ( 'NONE', 3,
 ( #80727, #71618, #56408, #87840 ),
 .UNSPECIFIED., .F., .F.,
 ( 4, 4 ),
 ( 0.000000000000000000, 0.0001000000000000028644 ),
 .UNSPECIFIED. ) ;
#13013=CARTESIAN_POINT ( 'NONE',  ( -99.64934318012689118, -25.30535455722350591, 4.927356316503054501 ) ) ;
#13015=EDGE_LOOP ( 'NONE', ( #14653, #17224, #83306, #25811 ) ) ;
#13016=CARTESIAN_POINT ( 'NONE',  ( -81.42380231474228935, -25.31401921878147832, 5.197788989978542773 ) ) ;
#13018=EDGE_CURVE ( 'NONE', #79516, #69040, #97926, .T. ) ;
#13019=EDGE_CURVE ( 'NONE', #39486, #29468, #67504, .T. ) ;
#13020=CARTESIAN_POINT ( 'NONE',  ( -57.52207137348256794, -23.48786465467241413, 11.44779295918254647 ) ) ;
#13021=ORIENTED_EDGE ( 'NONE', *, *, #69062, .T. ) ;
#13022=CARTESIAN_POINT ( 'NONE',  ( -40.01839366089613748, -25.30507950832802777, 5.509688047871486027 ) ) ;
#13023=CARTESIAN_POINT ( 'NONE',  ( -21.97457344801873447, 3.670769625195870134, -1.500000000000002220 ) ) ;
#13025=EDGE_CURVE ( 'NONE', #88628, #19742, #11863, .T. ) ;
#13027=CARTESIAN_POINT ( 'NONE',  ( -74.22287095715006444, -23.47596703998600631, 11.44779298504227860 ) ) ;
#13028=CARTESIAN_POINT ( 'NONE',  ( -75.52287095715007581, -29.50248528299804818, 1.056150453629038477 ) ) ;
#13029=CARTESIAN_POINT ( 'NONE',  ( -25.67560423947781700, -24.83136250832902547, 3.472477514678372845 ) ) ;
#13031=CARTESIAN_POINT ( 'NONE',  ( -61.64687923781919920, -29.50249039766296022, 3.409318347773680369 ) ) ;
#13035=CARTESIAN_POINT ( 'NONE',  ( 13.27039818535887505, -14.28956163997708906, 11.49999999999998934 ) ) ;
#13037=CARTESIAN_POINT ( 'NONE',  ( -3.867184171070207288, -21.11305558764578194, 11.49999999999998934 ) ) ;
#13041=CARTESIAN_POINT ( 'NONE',  ( -18.69919181139871966, -13.08804974640095686, -1.500000000000002220 ) ) ;
#13044=CARTESIAN_POINT ( 'NONE',  ( -96.58459092476410035, -24.66019654487199375, 8.947790411086115725 ) ) ;
#13045=CARTESIAN_POINT ( 'NONE',  ( -61.52287095715006160, -29.50248528299804818, 1.056150453629034924 ) ) ;
#13046=CARTESIAN_POINT ( 'NONE',  ( 1.534201407001029027, 19.92515851932037663, 11.49999999999999645 ) ) ;
#13047=CARTESIAN_POINT ( 'NONE',  ( -89.67764846858844408, -25.06732983082694943, 7.447789526168955732 ) ) ;
#13048=B_SPLINE_CURVE_WITH_KNOTS ( 'NONE', 3,
 ( #25826, #34445, #97334, #74005 ),
 .UNSPECIFIED., .F., .F.,
 ( 4, 4 ),
 ( 0.000000000000000000, 9.999999999998897304E-05 ),
 .UNSPECIFIED. ) ;
#13049=CARTESIAN_POINT ( 'NONE',  ( -117.6228709571500559, -24.64965695001469115, 8.947790433994175174 ) ) ;
#13050=CARTESIAN_POINT ( 'NONE',  ( -48.59340580069252269, -24.15543982623907127, -0.2315651400026527418 ) ) ;
#13051=ORIENTED_EDGE ( 'NONE', *, *, #56102, .T. ) ;
#13052=CARTESIAN_POINT ( 'NONE',  ( -26.29825405928423265, -24.66912159618280143, 2.250704355267874046 ) ) ;
#13053=FACE_OUTER_BOUND ( 'NONE', #30344, .T. ) ;
#13054=CARTESIAN_POINT ( 'NONE',  ( -14.78470843206283902, -15.91074852019131924, -1.500000000000002220 ) ) ;
#13055=LINE ( 'NONE', #36903, #7460 ) ;
#13056=CARTESIAN_POINT ( 'NONE',  ( 4.865394487973861537, 18.91859722749940786, -1.500000000000002220 ) ) ;
#13057=CARTESIAN_POINT ( 'NONE',  ( -34.52287095715006160, -23.48783264083359867, -1.443836473376372442 ) ) ;
#13058=B_SPLINE_CURVE_WITH_KNOTS ( 'NONE', 3,
 ( #21673, #51656, #82595, #68375, #44035, #53660 ),
 .UNSPECIFIED., .F., .F.,
 ( 4, 2, 4 ),
 ( 0.000000000000000000, 0.001380901958385399603, 0.002761803916770799207 ),
 .UNSPECIFIED. ) ;
#13061=FACE_OUTER_BOUND ( 'NONE', #37941, .T. ) ;
#13062=CARTESIAN_POINT ( 'NONE',  ( -40.55620429048340014, -23.47593901973091235, -1.443836447539011525 ) ) ;
#13063=CARTESIAN_POINT ( 'NONE',  ( 14.40702264168333890, -14.58922348230443689, 11.49999999999999645 ) ) ;
#13064=CARTESIAN_POINT ( 'NONE',  ( -49.34333941570991300, -25.27829611938825494, 5.818708551465133105 ) ) ;
#13067=CARTESIAN_POINT ( 'NONE',  ( -110.2093792378191921, -25.29160350784524880, 5.585409231008217290 ) ) ;
#13068=CARTESIAN_POINT ( 'NONE',  ( -106.6228709571500275, -23.95044443724992789, 10.65354141964649592 ) ) ;
#13069=DIRECTION ( 'NONE',  ( -3.773278334453079618E-23, 0.9999999999976377785, 2.173523156925979975E-06 ) ) ;
#13070=CARTESIAN_POINT ( 'NONE',  ( -61.59189125704995860, -25.07259839747099051, 7.371166918563575976 ) ) ;
#13074=CARTESIAN_POINT ( 'NONE',  ( -17.35246277222573141, 15.15038115719275424, 11.49999999999999645 ) ) ;
#13075=CARTESIAN_POINT ( 'NONE',  ( 6.015242202445381992, 21.98585358372262633, 11.49999999999998934 ) ) ;
#13076=CARTESIAN_POINT ( 'NONE',  ( -121.5228709571500616, -29.50247984919015209, -1.443849546365046699 ) ) ;
#13077=CARTESIAN_POINT ( 'NONE',  ( -49.21454750704995007, -25.13877828889947352, 7.069183601642414772 ) ) ;
#13078=CARTESIAN_POINT ( 'NONE',  ( -50.19553086926238450, -25.19638685952546808, 3.303372276271722363 ) ) ;
#13079=CARTESIAN_POINT ( 'NONE',  ( -64.52287095715006160, -24.65952944569304606, 1.056160979905695463 ) ) ;
#13080=CARTESIAN_POINT ( 'NONE',  ( -104.5228709571500758, -23.47596703998600631, 11.44779298504228215 ) ) ;
#13082=CARTESIAN_POINT ( 'NONE',  ( 19.28182042344761626, 10.37885539243483812, 11.49999999999998934 ) ) ;
#13083=CARTESIAN_POINT ( 'NONE',  ( -87.52287095715006160, -24.65952944569304606, 1.056160979905700570 ) ) ;
#13084=EDGE_CURVE ( 'NONE', #61918, #72942, #20803, .T. ) ;
#13085=CARTESIAN_POINT ( 'NONE',  ( -58.87764846857956513, -25.14083923594470704, 2.947789366366647901 ) ) ;
#13086=FACE_OUTER_BOUND ( 'NONE', #72828, .T. ) ;
#13087=DIRECTION ( 'NONE',  ( 3.773278334444166432E-23, -1.000000000000000000, 0.000000000000000000 ) ) ;
#13088=CARTESIAN_POINT ( 'NONE',  ( -45.52287095715006160, -29.50248789122583659, 2.256150453626215580 ) ) ;
#13089=ORIENTED_EDGE ( 'NONE', *, *, #42097, .T. ) ;
#13090=CARTESIAN_POINT ( 'NONE',  ( 6.539103723289373171, -19.38406401830294712, -1.500000000000002220 ) ) ;
#13092=VERTEX_POINT ( 'NONE', #28927 ) ;
#13093=ORIENTED_EDGE ( 'NONE', *, *, #8136, .F. ) ;
#13095=CARTESIAN_POINT ( 'NONE',  ( -8.820007276677138464, 21.28423624206370945, 11.49999999999998934 ) ) ;
#13096=CARTESIAN_POINT ( 'NONE',  ( -61.65508124498639120, -23.48783264082476663, -1.443836473390096575 ) ) ;
#13097=CARTESIAN_POINT ( 'NONE',  ( 20.02926185082240451, -2.967945350358753398, -1.500000000000002220 ) ) ;
#13099=EDGE_CURVE ( 'NONE', #26794, #12874, #34770, .T. ) ;
#13103=EDGE_CURVE ( 'NONE', #56351, #80901, #82711, .T. ) ;
#13104=AXIS2_PLACEMENT_3D ( 'NONE', #75304, #89546, #5802 ) ;
#13105=CARTESIAN_POINT ( 'NONE',  ( -95.55038110527486594, -24.40034930558991633, 0.3402023900116099009 ) ) ;
#13106=CARTESIAN_POINT ( 'NONE',  ( -53.64457961018205623, -23.96169478059712787, 10.65365249895718591 ) ) ;
#13107=CARTESIAN_POINT ( 'NONE',  ( 11.86944616785735818, -17.87650476368427732, 11.49999999999999645 ) ) ;
#13108=VERTEX_POINT ( 'NONE', #13188 ) ;
#13109=CARTESIAN_POINT ( 'NONE',  ( -128.6228709571500417, -23.94994826722516379, -0.6494450866351710872 ) ) ;
#13110=AXIS2_PLACEMENT_3D ( 'NONE', #60559, #4266, #28099 ) ;
#13112=ORIENTED_EDGE ( 'NONE', *, *, #47493, .F. ) ;
#13113=CARTESIAN_POINT ( 'NONE',  ( 16.16129659511371131, 15.28805624652528472, 11.49999999999998934 ) ) ;
#13114=CARTESIAN_POINT ( 'NONE',  ( 20.27745880512110688, -4.159726151199424571, -1.500000000000002220 ) ) ;
#13115=VERTEX_POINT ( 'NONE', #37041 ) ;
#13117=ORIENTED_EDGE ( 'NONE', *, *, #14952, .F. ) ;
#13118=CARTESIAN_POINT ( 'NONE',  ( -81.52287095715007581, -23.96127896942134683, -0.6493128930938705246 ) ) ;
#13120=CARTESIAN_POINT ( 'NONE',  ( 19.95448254803897115, -6.385634049875297258, -1.500000000000002220 ) ) ;
#13121=EDGE_CURVE ( 'NONE', #29369, #8268, #89340, .T. ) ;
#13122=CARTESIAN_POINT ( 'NONE',  ( 6.821863743248424150, 20.85434273413645911, 11.49999999999999645 ) ) ;
#13124=CARTESIAN_POINT ( 'NONE',  ( -8.307687032909205627, 20.95097986170506488, 11.49999999999998934 ) ) ;
#13125=CARTESIAN_POINT ( 'NONE',  ( 15.04517842881462819, -14.58609674458608829, 11.49999999999998934 ) ) ;
#13127=CARTESIAN_POINT ( 'NONE',  ( -52.62287095715005592, -24.66019654487199020, 8.947790411086135265 ) ) ;
#13129=ORIENTED_EDGE ( 'NONE', *, *, #86725, .T. ) ;
#13130=EDGE_CURVE ( 'NONE', #26963, #11989, #4611, .T. ) ;
#13131=ORIENTED_EDGE ( 'NONE', *, *, #20480, .F. ) ;
#13132=ORIENTED_EDGE ( 'NONE', *, *, #33105, .F. ) ;
#13135=CARTESIAN_POINT ( 'NONE',  ( -4.253298834618286506, 21.06115358058179154, -1.500000000000002220 ) ) ;
#13136=CARTESIAN_POINT ( 'NONE',  ( -86.62287095714999907, -24.35013146730203815, 9.818937971375108376 ) ) ;
#13137=ORIENTED_EDGE ( 'NONE', *, *, #99800, .T. ) ;
#13138=CARTESIAN_POINT ( 'NONE',  ( -20.28541985502614509, -5.886007371444655689, 11.49999999999998934 ) ) ;
#13139=CARTESIAN_POINT ( 'NONE',  ( -59.56094173781918499, -25.20074414198133539, 3.409327697718782080 ) ) ;
#13140=CARTESIAN_POINT ( 'NONE',  ( -64.53961665416358073, -24.51314013834315730, 0.6176544820404094027 ) ) ;
#13141=CARTESIAN_POINT ( 'NONE',  ( -64.55620429048340725, -23.48783264082478084, -1.443836473390069264 ) ) ;
#13143=CARTESIAN_POINT ( 'NONE',  ( -123.5228709571501042, -23.48783264082477018, -1.443836473390084141 ) ) ;
#13144=CARTESIAN_POINT ( 'NONE',  ( 14.84500176111689207, -16.38379996218902335, -1.500000000000002220 ) ) ;
#13145=DIRECTION ( 'NONE',  ( 0.000000000000000000, 0.9999999999976377785, 2.173523156925979975E-06 ) ) ;
#13146=B_SPLINE_CURVE_WITH_KNOTS ( 'NONE', 3,
 ( #17297, #48768, #32021, #47761, #48262, #78676 ),
 .UNSPECIFIED., .F., .F.,
 ( 4, 2, 4 ),
 ( 0.000000000000000000, 0.001380764517854768218, 0.002761529035709536437 ),
 .UNSPECIFIED. ) ;
#13147=EDGE_CURVE ( 'NONE', #8399, #72949, #20190, .T. ) ;
#13151=ADVANCED_FACE ( 'NONE', ( #53275 ), #24312, .T. ) ;
#13153=CARTESIAN_POINT ( 'NONE',  ( -19.08929872761019908, -3.557156390981079053, -1.500000000000002220 ) ) ;
#13154=CARTESIAN_POINT ( 'NONE',  ( 20.90283063341239966, -4.354886778353011856, 11.49999999999998934 ) ) ;
#13155=CARTESIAN_POINT ( 'NONE',  ( -66.55620429048339304, -23.48783264082478794, -1.443836473390067265 ) ) ;
#13156=CARTESIAN_POINT ( 'NONE',  ( -49.89149569650673754, -25.11539320716599377, 2.804431449967496714 ) ) ;
#13157=B_SPLINE_CURVE_WITH_KNOTS ( 'NONE', 3,
 ( #33558, #73621, #49804, #56416 ),
 .UNSPECIFIED., .F., .F.,
 ( 4, 4 ),
 ( 0.000000000000000000, 0.0001000000000000028644 ),
 .UNSPECIFIED. ) ;
#13158=EDGE_CURVE ( 'NONE', #23352, #34952, #7018, .T. ) ;
#13159=CARTESIAN_POINT ( 'NONE',  ( -86.52287095715006160, -24.64898659630367916, 1.056161002820827921 ) ) ;
#13160=CARTESIAN_POINT ( 'NONE',  ( -69.55126625704997423, -25.15208592601422311, 3.076695591939294427 ) ) ;
#13161=CARTESIAN_POINT ( 'NONE',  ( 5.572475817582897228, 21.94689365879375131, -1.500000000000002220 ) ) ;
#13164=FACE_OUTER_BOUND ( 'NONE', #53955, .T. ) ;
#13165=CARTESIAN_POINT ( 'NONE',  ( -15.51018552496569392, -12.33189742059753868, 11.49999999999999645 ) ) ;
#13167=CARTESIAN_POINT ( 'NONE',  ( -119.5562042904833930, -24.66019654487200086, 8.947790411086121054 ) ) ;
#13169=CARTESIAN_POINT ( 'NONE',  ( -68.55620429048339304, -24.66019654487199020, 8.947790411086131712 ) ) ;
#13170=CARTESIAN_POINT ( 'NONE',  ( -28.67105337545913812, -25.26026344719939942, 1.897770660017422673 ) ) ;
#13171=CARTESIAN_POINT ( 'NONE',  ( -100.5528973737291238, -25.17353343482556483, 7.099974540203241702 ) ) ;
#13172=CARTESIAN_POINT ( 'NONE',  ( -7.466173891270859286, -20.28576548065916541, -1.500000000000002220 ) ) ;
#13173=CARTESIAN_POINT ( 'NONE',  ( -99.62287095715007013, -24.51283580621365843, 0.6167428607019790343 ) ) ;
#13174=CARTESIAN_POINT ( 'NONE',  ( -19.24332624019526961, -2.196797614219411443, -1.500000000000002220 ) ) ;
#13175=CARTESIAN_POINT ( 'NONE',  ( -108.6228709571500559, -29.50247984919015209, -1.443849546365048253 ) ) ;
#13176=DIRECTION ( 'NONE',  ( -1.000000000000000000, -3.773278334444166432E-23, -8.201307841325785021E-29 ) ) ;
#13177=CARTESIAN_POINT ( 'NONE',  ( -17.21045110277357182, -9.822940424218707278, 11.49999999999998934 ) ) ;
#13179=VERTEX_POINT ( 'NONE', #93824 ) ;
#13180=CARTESIAN_POINT ( 'NONE',  ( -11.05657426389776354, 17.00066307926000420, 11.49999999999999645 ) ) ;
#13183=ORIENTED_EDGE ( 'NONE', *, *, #27502, .T. ) ;
#13184=CARTESIAN_POINT ( 'NONE',  ( -102.5508160338511914, -24.35071581493543746, 9.817618358456027039 ) ) ;
#13185=CARTESIAN_POINT ( 'NONE',  ( -102.5228709571501042, -23.48783264083375144, -1.443836473376139740 ) ) ;
#13186=LINE ( 'NONE', #28418, #74283 ) ;
#13188=CARTESIAN_POINT ( 'NONE',  ( -70.62287095715005592, -25.00158670708909270, 2.256160236439166855 ) ) ;
#13189=CARTESIAN_POINT ( 'NONE',  ( -0.1815635828756200498, -20.05798930676971636, -1.500000000000002220 ) ) ;
#13190=CARTESIAN_POINT ( 'NONE',  ( -85.52287095715006160, -24.14321612903117042, -0.2833117244520886868 ) ) ;
#13191=VERTEX_POINT ( 'NONE', #14694 ) ;
#13193=CARTESIAN_POINT ( 'NONE',  ( 4.317061085376620255, -22.40314112565372540, 11.49999999999999645 ) ) ;
#13194=CARTESIAN_POINT ( 'NONE',  ( -49.84984290111637506, -25.26258851161916397, 4.578680057367619405 ) ) ;
#13195=DIRECTION ( 'NONE',  ( -3.773278334453079618E-23, 0.9999999999976377785, 2.173523156925979975E-06 ) ) ;
#13197=CARTESIAN_POINT ( 'NONE',  ( -76.52287095715007581, -23.47596703998600631, 11.44779298504228571 ) ) ;
#13199=AXIS2_PLACEMENT_3D ( 'NONE', #61086, #84900, #71065 ) ;
#13200=CARTESIAN_POINT ( 'NONE',  ( -5.254942042970298210, 21.81482460008805546, 11.49999999999999645 ) ) ;
#13201=B_SPLINE_CURVE_WITH_KNOTS ( 'NONE', 3,
 ( #25548, #56517, #87446, #89331, #74107, #97438 ),
 .UNSPECIFIED., .F., .F.,
 ( 4, 2, 4 ),
 ( 6.384118678610533503E-06, 0.001386860460828370214, 0.002767336802978130183 ),
 .UNSPECIFIED. ) ;
#13203=EDGE_LOOP ( 'NONE', ( #53550, #67155, #38976, #98236 ) ) ;
#13204=ADVANCED_FACE ( 'NONE', ( #69986 ), #78082, .F. ) ;
#13205=CARTESIAN_POINT ( 'NONE',  ( 19.78452974690265975, -4.759501717958375622, -1.500000000000002220 ) ) ;
#13206=B_SPLINE_CURVE_WITH_KNOTS ( 'NONE', 3,
 ( #17228, #49204, #18725, #80634, #22932, #64442 ),
 .UNSPECIFIED., .F., .F.,
 ( 4, 2, 4 ),
 ( 1.570887131794638196E-05, 0.001396322306279761940, 0.002776935741241577573 ),
 .UNSPECIFIED. ) ;
#13208=EDGE_CURVE ( 'NONE', #22696, #77182, #9088, .T. ) ;
#13209=B_SPLINE_CURVE_WITH_KNOTS ( 'NONE', 3,
 ( #93878, #71557, #55336, #71053 ),
 .UNSPECIFIED., .F., .F.,
 ( 4, 4 ),
 ( 0.000000000000000000, 9.999999999998897304E-05 ),
 .UNSPECIFIED. ) ;
#13210=CARTESIAN_POINT ( 'NONE',  ( 8.986065527603487979, -21.13286776747340667, -1.500000000000002220 ) ) ;
#13212=ADVANCED_FACE ( 'NONE', ( #47664 ), #30922, .T. ) ;
#13213=VERTEX_POINT ( 'NONE', #39542 ) ;
#13214=CARTESIAN_POINT ( 'NONE',  ( -37.62287095715005592, -24.64898659630367206, 1.056161002820819261 ) ) ;
#13216=CARTESIAN_POINT ( 'NONE',  ( -77.52287095715006160, -24.64965694238575011, 8.947790433994198267 ) ) ;
#13217=CARTESIAN_POINT ( 'NONE',  ( -33.62287095715005592, -29.50247984919015209, -1.443849546365062242 ) ) ;
#13218=CARTESIAN_POINT ( 'NONE',  ( -9.505907188867841029, -19.02311915605711690, 11.49999999999999645 ) ) ;
#13220=EDGE_LOOP ( 'NONE', ( #33542, #21108, #12670, #37227 ) ) ;
#13221=CARTESIAN_POINT ( 'NONE',  ( -21.91529987491217923, -3.391794311424265018, -1.500000000000002220 ) ) ;
#13223=CARTESIAN_POINT ( 'NONE',  ( -18.82610421443283499, -8.410905081555696938, 11.49999999999998934 ) ) ;
#13225=EDGE_LOOP ( 'NONE', ( #99354, #22487, #96559, #98560 ) ) ;
#13227=EDGE_CURVE ( 'NONE', #39701, #59550, #90088, .T. ) ;
#13230=ORIENTED_EDGE ( 'NONE', *, *, #78327, .T. ) ;
#13231=ORIENTED_EDGE ( 'NONE', *, *, #96094, .T. ) ;
#13232=CARTESIAN_POINT ( 'NONE',  ( -72.52287095715007581, -24.64965694238575011, 8.947790433994200043 ) ) ;
#13235=CARTESIAN_POINT ( 'NONE',  ( 8.872108392497455753, -18.76566404461018678, -1.500000000000002220 ) ) ;
#13236=CARTESIAN_POINT ( 'NONE',  ( -14.78470843206283902, -15.91074852019131924, 11.49999999999999645 ) ) ;
#13238=CARTESIAN_POINT ( 'NONE',  ( -39.48051905766907765, -25.25935834831543048, 3.941559143231549545 ) ) ;
#13239=CARTESIAN_POINT ( 'NONE',  ( -98.89667130318164823, -25.24584994799474558, 6.210313119106261048 ) ) ;
#13240=CARTESIAN_POINT ( 'NONE',  ( -115.5956203964720146, -23.48783264082477018, -1.443836473390087916 ) ) ;
#13241=CARTESIAN_POINT ( 'NONE',  ( -16.84940295534276800, 14.81145437567392698, -1.500000000000002220 ) ) ;
#13242=CARTESIAN_POINT ( 'NONE',  ( -51.02503725990638372, -25.26334701977532049, 4.507473529586822458 ) ) ;
#13243=ORIENTED_EDGE ( 'NONE', *, *, #28984, .T. ) ;
#13244=CARTESIAN_POINT ( 'NONE',  ( -98.52287095715006160, -23.95044443724992078, 10.65354141964649237 ) ) ;
#13251=B_SPLINE_CURVE_WITH_KNOTS ( 'NONE', 3,
 ( #82430, #20524, #51497, #67230, #28652, #90544 ),
 .UNSPECIFIED., .F., .F.,
 ( 4, 2, 4 ),
 ( 6.391158118952234240E-06, 0.001387004593080775738, 0.002767618028042598960 ),
 .UNSPECIFIED. ) ;
#13252=CARTESIAN_POINT ( 'NONE',  ( -100.1366382179432293, -25.31290980448949313, 5.258043518187221821 ) ) ;
#13253=ORIENTED_EDGE ( 'NONE', *, *, #69404, .T. ) ;
#13254=CARTESIAN_POINT ( 'NONE',  ( -1.825377252022436281, -21.23478267787193730, -1.500000000000002220 ) ) ;
#13255=ORIENTED_EDGE ( 'NONE', *, *, #23875, .T. ) ;
#13257=CARTESIAN_POINT ( 'NONE',  ( 3.267597511969735802, 21.59432767039258394, 11.49999999999998934 ) ) ;
#13258=CARTESIAN_POINT ( 'NONE',  ( -124.6228709571500701, -23.47596703998600631, 11.44779298504227860 ) ) ;
#13259=CARTESIAN_POINT ( 'NONE',  ( -6.316168294299441932, 21.79233575779346310, -1.500000000000002220 ) ) ;
#13260=CARTESIAN_POINT ( 'NONE',  ( -41.30067620550419605, -25.18430957957208705, 3.692502768481106035 ) ) ;
#13261=CARTESIAN_POINT ( 'NONE',  ( -28.52287095715007226, -23.32374950011072912, -1.443835813551990643 ) ) ;
#13262=CARTESIAN_POINT ( 'NONE',  ( 9.922928194174257754, 19.57116106031148561, -1.500000000000002220 ) ) ;
#13263=CARTESIAN_POINT ( 'NONE',  ( -91.52287095715006160, -29.50247984919015209, -1.443849546365051806 ) ) ;
#13264=ORIENTED_EDGE ( 'NONE', *, *, #52474, .F. ) ;
#13265=CARTESIAN_POINT ( 'NONE',  ( -40.41259864834562165, -25.29360172625626291, 5.542179568230306330 ) ) ;
#13268=CARTESIAN_POINT ( 'NONE',  ( -84.59178562529271517, -24.15620529776628445, 10.23563542870660292 ) ) ;
#13270=CARTESIAN_POINT ( 'NONE',  ( -0.07959803473139435981, -22.01954088903998397, 0.3010598746230524481 ) ) ;
#13271=CARTESIAN_POINT ( 'NONE',  ( 6.361473516681357410, -20.28576754457002451, 11.49999999999998934 ) ) ;
#13272=CARTESIAN_POINT ( 'NONE',  ( -112.6283935189997436, -23.96119346886881729, -0.6495511937831842664 ) ) ;
#13273=CARTESIAN_POINT ( 'NONE',  ( -26.10669942825130363, -24.75186453689402200, 4.499505972768075956 ) ) ;
#13274=EDGE_CURVE ( 'NONE', #43699, #64811, #61483, .T. ) ;
#13275=CARTESIAN_POINT ( 'NONE',  ( -85.51040508421080233, -24.15503026093913519, -0.2815557561904480921 ) ) ;
#13276=CARTESIAN_POINT ( 'NONE',  ( -33.60984950083365419, -23.73766607897670866, -1.055555164236444909 ) ) ;
#13278=B_SPLINE_SURFACE_WITH_KNOTS ( 'NONE', 3, 3, ( 
 ( #55992, #71706, #48874, #49883 ),
 ( #79801, #10298, #42280, #73210 ),
 ( #24514, #55482, #16906, #47869 ),
 ( #34644, #29010, #81310, #51363 ),
 ( #52359, #28512, #65613, #59475 ),
 ( #27025, #50869, #74685, #90416 ),
 ( #58983, #81808, #88929, #5180 ) ),
 .UNSPECIFIED., .F., .F., .F.,
 ( 4, 3, 4 ),
 ( 4, 4 ),
 ( 0.7945040050992235869, 0.8970133687736494554, 0.9995227324480753239 ),
 ( 0.1295269118291874078, 0.1305994346019532237 ),
 .UNSPECIFIED. ) ;
#13279=CARTESIAN_POINT ( 'NONE',  ( -39.62287095715005592, -24.66019654487199020, 8.947790411086135265 ) ) ;
#13280=ORIENTED_EDGE ( 'NONE', *, *, #38333, .F. ) ;
#13281=CARTESIAN_POINT ( 'NONE',  ( 19.11985901488480621, -4.296470200863222288, 11.49999999999999645 ) ) ;
#13282=CARTESIAN_POINT ( 'NONE',  ( -99.30758664999683560, -25.30967407356133947, 4.614854304310689770 ) ) ;
#13283=CARTESIAN_POINT ( 'NONE',  ( -70.34543693012690824, -29.50249942614373921, 7.563164501610022405 ) ) ;
#13284=EDGE_LOOP ( 'NONE', ( #25096, #44203, #54203, #96164 ) ) ;
#13285=DIRECTION ( 'NONE',  ( 1.000000000000000000, 3.773278334444167608E-23, 8.201307833595939069E-29 ) ) ;
#13286=CARTESIAN_POINT ( 'NONE',  ( -99.29687923781919778, -25.31439739983868975, 6.149712066081883144 ) ) ;
#13287=CARTESIAN_POINT ( 'NONE',  ( -62.92287095715006018, -23.47596703998600276, 11.44779298504227683 ) ) ;
#13288=CARTESIAN_POINT ( 'NONE',  ( -60.52287095715006870, -24.83602698348160587, 1.605859176311257519 ) ) ;
#13289=CARTESIAN_POINT ( 'NONE',  ( 6.578723047037327909, -18.57437435983987584, 11.49999999999998934 ) ) ;
#13290=ORIENTED_EDGE ( 'NONE', *, *, #81577, .T. ) ;
#13291=AXIS2_PLACEMENT_3D ( 'NONE', #90682, #98784, #35898 ) ;
#13297=CARTESIAN_POINT ( 'NONE',  ( -54.52287095715009002, -23.72773821059537269, 11.05748984161097326 ) ) ;
#13298=CARTESIAN_POINT ( 'NONE',  ( -103.6228709571500985, -23.73934037231757799, 11.05740245334328442 ) ) ;
#13299=CARTESIAN_POINT ( 'NONE',  ( -120.5228709571500616, -23.47596703998600631, 11.44779298504227860 ) ) ;
#13300=CARTESIAN_POINT ( 'NONE',  ( -118.5922137762087232, -23.73766607897671221, -1.055555164236448684 ) ) ;
#13301=CARTESIAN_POINT ( 'NONE',  ( -45.55620429048338593, -24.99156044556202616, 7.747789690856173195 ) ) ;
#13302=CARTESIAN_POINT ( 'NONE',  ( -69.64006105340874342, -25.24515098634607568, 5.573124385056173580 ) ) ;
#13304=CARTESIAN_POINT ( 'NONE',  ( -0.003041637939312698616, 19.98351707251910980, -1.500000000000002220 ) ) ;
#13305=CARTESIAN_POINT ( 'NONE',  ( -32.52287095715006160, -24.64898659630528854, 1.056161002820817485 ) ) ;
#13306=CARTESIAN_POINT ( 'NONE',  ( -0.06514381684952065543, -22.20666209822921999, 9.487281999122094689 ) ) ;
#13308=CARTESIAN_POINT ( 'NONE',  ( -29.52287095715004739, -23.86438995984020650, -0.6496299998811901899 ) ) ;
#13310=VECTOR ( 'NONE', #79676, 1000.000000000000114 ) ;
#13312=CARTESIAN_POINT ( 'NONE',  ( -119.6248184345861887, -24.34968618360934656, 0.1864209137778924386 ) ) ;
#13313=CARTESIAN_POINT ( 'NONE',  ( -80.63291137919141249, -24.52399227489127398, 9.353111116836524630 ) ) ;
#13314=PLANE ( 'NONE',  #93158 ) ;
#13315=CARTESIAN_POINT ( 'NONE',  ( -81.58822170641624894, -24.34968618360933945, 0.1864209137778954084 ) ) ;
#13316=CARTESIAN_POINT ( 'NONE',  ( -27.99826093239865443, -24.60093894690410465, 1.648430988000137765 ) ) ;
#13318=ORIENTED_EDGE ( 'NONE', *, *, #69941, .T. ) ;
#13320=CARTESIAN_POINT ( 'NONE',  ( -127.5554375122736843, -24.34968618360935011, 0.1864209137778923830 ) ) ;
#13321=VERTEX_POINT ( 'NONE', #48676 ) ;
#13323=CARTESIAN_POINT ( 'NONE',  ( -18.77428246231291808, -7.638711222589018135, -1.500000000000002220 ) ) ;
#13324=CARTESIAN_POINT ( 'NONE',  ( -69.92341571696384506, -25.31508615006725194, 4.890982526048191836 ) ) ;
#13330=DIRECTION ( 'NONE',  ( 0.000000000000000000, -2.173523156925980399E-06, 0.9999999999976378895 ) ) ;
#13331=CARTESIAN_POINT ( 'NONE',  ( -105.5228709571500616, -25.00158670708909980, 2.256160236439166411 ) ) ;
#13332=CARTESIAN_POINT ( 'NONE',  ( 19.70663390988245922, 3.666079223618853966, -1.500000000000002220 ) ) ;
#13334=CARTESIAN_POINT ( 'NONE',  ( 20.99820426035194032, -0.1900765340283884497, 11.49999999999999645 ) ) ;
#13335=CARTESIAN_POINT ( 'NONE',  ( -29.24562161810074556, -25.21411260810315369, 5.231851746718979790 ) ) ;
#13336=CARTESIAN_POINT ( 'NONE',  ( -70.49527151980225881, -24.63419186844611986, 9.035850630976923981 ) ) ;
#13337=CARTESIAN_POINT ( 'NONE',  ( 0.6065052782250800467, 22.08157775750015617, -1.500000000000002220 ) ) ;
#13339=B_SPLINE_CURVE_WITH_KNOTS ( 'NONE', 3,
 ( #80219, #87325, #11209, #2112, #64027, #72120 ),
 .UNSPECIFIED., .F., .F.,
 ( 4, 2, 4 ),
 ( 0.000000000000000000, 0.001380764517854763231, 0.002761529035709526462 ),
 .UNSPECIFIED. ) ;
#13340=CARTESIAN_POINT ( 'NONE',  ( 19.83930831332124001, -5.160774681608516268, 11.49999999999998934 ) ) ;
#13341=DIRECTION ( 'NONE',  ( -3.773278334453079618E-23, 0.9999999999976377785, 2.173523156925978705E-06 ) ) ;
#13342=VECTOR ( 'NONE', #73585, 1000.000000000000114 ) ;
#13343=DIRECTION ( 'NONE',  ( 3.773278334444166432E-23, -1.000000000000000000, 0.000000000000000000 ) ) ;
#13344=FACE_OUTER_BOUND ( 'NONE', #87300, .T. ) ;
#13345=ORIENTED_EDGE ( 'NONE', *, *, #35183, .F. ) ;
#13346=CARTESIAN_POINT ( 'NONE',  ( -87.62287095715004170, -29.50250243563736774, 8.947779886222139822 ) ) ;
#13347=CARTESIAN_POINT ( 'NONE',  ( -31.48246563699567346, -24.51314013834316086, 0.6176544820404139546 ) ) ;
#13348=VERTEX_POINT ( 'NONE', #66275 ) ;
#13351=CARTESIAN_POINT ( 'NONE',  ( -124.9228709571500673, -23.47596703998600987, 11.44779298504228038 ) ) ;
#13354=CARTESIAN_POINT ( 'NONE',  ( -3.146292006899429783, -20.37002610441940220, -1.500000000000002220 ) ) ;
#13355=CARTESIAN_POINT ( 'NONE',  ( -20.54952838774410750, 6.582847151591199264, 11.49999999999999645 ) ) ;
#13356=VERTEX_POINT ( 'NONE', #20071 ) ;
#13357=CARTESIAN_POINT ( 'NONE',  ( -99.13318064690763265, -25.27852886613005268, 4.186868528538305156 ) ) ;
#13358=CARTESIAN_POINT ( 'NONE',  ( -55.52287095715006870, -29.50250243563736774, 8.947779886222145151 ) ) ;
#13359=CARTESIAN_POINT ( 'NONE',  ( 16.92800457317958518, -14.60656088873787262, -1.500000000000002220 ) ) ;
#13360=CARTESIAN_POINT ( 'NONE',  ( -79.53472330195882023, -25.27874982639352908, 6.603900679166175181 ) ) ;
#13361=CARTESIAN_POINT ( 'NONE',  ( -65.52287095715006160, -23.48786465467241058, 11.44779295918254647 ) ) ;
#13363=B_SPLINE_CURVE_WITH_KNOTS ( 'NONE', 3,
 ( #56758, #87687, #20652, #37395 ),
 .UNSPECIFIED., .F., .F.,
 ( 4, 4 ),
 ( 0.000000000000000000, 0.0001000000000000028644 ),
 .UNSPECIFIED. ) ;
#13364=CARTESIAN_POINT ( 'NONE',  ( -35.52287095715006870, -24.99132157543083821, 2.256160258750667502 ) ) ;
#13366=VECTOR ( 'NONE', #43409, 1000.000000000000114 ) ;
#13367=CARTESIAN_POINT ( 'NONE',  ( 11.28189403632909915, 17.58240144430209995, -1.500000000000002220 ) ) ;
#13368=EDGE_LOOP ( 'NONE', ( #57995, #65708, #72116, #67408 ) ) ;
#13369=CARTESIAN_POINT ( 'NONE',  ( -86.62359145833659113, -24.65952944569304606, 1.056160979905700126 ) ) ;
#13371=ORIENTED_EDGE ( 'NONE', *, *, #3410, .F. ) ;
#13372=CARTESIAN_POINT ( 'NONE',  ( -100.5618449191744475, -23.48786465467241413, 11.44779295918254469 ) ) ;
#13373=CARTESIAN_POINT ( 'NONE',  ( -20.67868931609407213, -4.308284118179648736, -1.500000000000002220 ) ) ;
#13374=ORIENTED_EDGE ( 'NONE', *, *, #18950, .T. ) ;
#13375=CARTESIAN_POINT ( 'NONE',  ( -112.5228709571500616, -24.64965694238408034, 8.947790433994192938 ) ) ;
#13376=DIRECTION ( 'NONE',  ( -3.773278334453079030E-23, 0.9999999999976377785, 2.173523156925979128E-06 ) ) ;
#13377=CARTESIAN_POINT ( 'NONE',  ( -81.52287095715006160, -24.65952944569304606, 1.056160979905698794 ) ) ;
#13378=CARTESIAN_POINT ( 'NONE',  ( -76.51215162630506939, -23.96169478059713143, 10.65365249895718058 ) ) ;
#13379=CARTESIAN_POINT ( 'NONE',  ( -32.62287095715004881, -23.47593901973091235, -1.443836447539013301 ) ) ;
#13380=CARTESIAN_POINT ( 'NONE',  ( 21.64095104908334122, -2.195182070091274529, -1.500000000000002220 ) ) ;
#13381=CARTESIAN_POINT ( 'NONE',  ( -71.64734380851882634, -25.24674250085310234, 5.762066786199834922 ) ) ;
#13382=CARTESIAN_POINT ( 'NONE',  ( 10.93216147639808611, 19.43004700418156361, 11.49999999999999645 ) ) ;
#13383=ORIENTED_EDGE ( 'NONE', *, *, #77638, .F. ) ;
#13386=EDGE_CURVE ( 'NONE', #48183, #1913, #25047, .T. ) ;
#13387=CARTESIAN_POINT ( 'NONE',  ( -113.6228709571500559, -29.50248528299804818, 1.056150453629043584 ) ) ;
#13388=VERTEX_POINT ( 'NONE', #74361 ) ;
#13392=ORIENTED_EDGE ( 'NONE', *, *, #51968, .T. ) ;
#13396=LINE ( 'NONE', #75794, #10611 ) ;
#13397=PLANE ( 'NONE',  #87522 ) ;
#13398=AXIS2_PLACEMENT_3D ( 'NONE', #74101, #97431, #27918 ) ;
#13399=CARTESIAN_POINT ( 'NONE',  ( -13.40542139710017899, 13.98966777563825481, -1.500000000000002220 ) ) ;
#13401=CARTESIAN_POINT ( 'NONE',  ( -45.92287095715005307, -23.47596703998600276, 11.44779298504227683 ) ) ;
#13403=CARTESIAN_POINT ( 'NONE',  ( 15.36829964806744364, -11.83880051060199712, 11.49999999999999645 ) ) ;
#13405=VECTOR ( 'NONE', #41489, 1000.000000000000114 ) ;
#13406=EDGE_CURVE ( 'NONE', #47188, #49194, #86708, .T. ) ;
#13409=DIRECTION ( 'NONE',  ( -3.773278334453079618E-23, 0.9999999999976377785, 2.173523156925979552E-06 ) ) ;
#13411=CARTESIAN_POINT ( 'NONE',  ( -87.62287095714999907, -24.33927499327853639, 9.819080762295817166 ) ) ;
#13412=CARTESIAN_POINT ( 'NONE',  ( -17.52035102510334141, -8.822347199899118309, -1.500000000000002220 ) ) ;
#13413=B_SPLINE_SURFACE_WITH_KNOTS ( 'NONE', 3, 3, ( 
 ( #14253, #93378, #61954, #8158 ),
 ( #99978, #53342, #53841, #54842 ),
 ( #70554, #92880, #6651, #23359 ),
 ( #85268, #46216, #37607, #77150 ),
 ( #83771, #70053, #539, #31487 ),
 ( #54343, #52835, #15760, #62450 ),
 ( #30487, #84271, #84772, #85783 ),
 ( #1050, #46725, #68556, #16265 ),
 ( #78145, #7654, #99490, #38603 ),
 ( #29985, #22355, #45722, #76645 ),
 ( #7146, #38098, #69052, #61455 ),
 ( #92382, #15260, #69562, #9150 ),
 ( #18272, #64481, #72077, #47728 ),
 ( #71571, #34002, #80172, #93889 ),
 ( #40111, #33003, #2064, #49244 ),
 ( #10663, #41624, #17268, #94391 ),
 ( #55849, #32497, #86278, #48231 ),
 ( #49742, #55346, #78644, #80669 ),
 ( #95395, #71067, #48741, #87276 ),
 ( #87789, #17777, #79661, #11156 ),
 ( #10161, #86777, #79162, #1556 ),
 ( #42132, #2557, #63469, #64978 ),
 ( #73072, #94888, #24873, #9661 ),
 ( #40616, #63978, #25885, #25380 ),
 ( #33494, #56357, #3556, #56857 ) ),
 .UNSPECIFIED., .F., .F., .F.,
 ( 4, 3, 3, 3, 3, 3, 3, 3, 4 ),
 ( 4, 4 ),
 ( 0.0004766824943081664212, 0.1253574377757289138, 0.1877978154164393065, 0.2502381930571496715, 0.4999997036199911871, 0.7497612141828327026, 0.8122015918235430121, 0.8746419694642534326, 0.9995227247456741626 ),
 ( 0.0001139708429040862454, 0.005838217335517809428 ),
 .UNSPECIFIED. ) ;
#13414=CARTESIAN_POINT ( 'NONE',  ( -37.55620429048340725, -24.64898659630528144, 1.056161002820821260 ) ) ;
#13416=CARTESIAN_POINT ( 'NONE',  ( 20.98156868870745484, 4.911575462371418510, 11.49999999999998934 ) ) ;
#13417=CARTESIAN_POINT ( 'NONE',  ( -33.56120774392356054, -23.73791477778911130, 11.05961554403171299 ) ) ;
#13421=CARTESIAN_POINT ( 'NONE',  ( 20.85440106035463970, 9.703512019146668166, -1.500000000000002220 ) ) ;
#13425=CARTESIAN_POINT ( 'NONE',  ( -101.7776484685884100, -25.27307239909451653, 3.986250617436227550 ) ) ;
#13426=DIRECTION ( 'NONE',  ( -3.773278334453079618E-23, 0.9999999999976377785, 2.173523156925979975E-06 ) ) ;
#13427=CARTESIAN_POINT ( 'NONE',  ( -17.50950832565593984, 9.922426906265528146, 11.49999999999999645 ) ) ;
#13429=CARTESIAN_POINT ( 'NONE',  ( -32.57080280157106955, -23.48786465467240347, 11.44779295918255535 ) ) ;
#13432=CARTESIAN_POINT ( 'NONE',  ( -29.55620429048338949, -23.40360120717180692, 11.44779300713762638 ) ) ;
#13433=CARTESIAN_POINT ( 'NONE',  ( -111.0533842133887390, -25.18425641804806503, 3.566050094442076102 ) ) ;
#13434=CARTESIAN_POINT ( 'NONE',  ( 3.337697395173636394, -19.57427954046807983, -1.500000000000002220 ) ) ;
#13437=CARTESIAN_POINT ( 'NONE',  ( -3.970774856468506364, -19.35638658347046714, -1.500000000000002220 ) ) ;
#13440=DESIGN_CONTEXT ( 'detailed design', #94551, 'design' ) ;
#13443=CARTESIAN_POINT ( 'NONE',  ( 7.508984785159893427, -19.29828013722326929, 11.49999999999999645 ) ) ;
#13446=DIRECTION ( 'NONE',  ( 0.000000000000000000, -0.9999999999976377785, -2.173523156925979975E-06 ) ) ;
#13447=CARTESIAN_POINT ( 'NONE',  ( 9.518656604726816184, -20.62229310799655124, 11.49999999999999645 ) ) ;
#13451=EDGE_CURVE ( 'NONE', #92742, #58910, #99015, .T. ) ;
#13452=CARTESIAN_POINT ( 'NONE',  ( -63.63170861370627307, -24.34968618360933590, 0.1864209137778804204 ) ) ;
#13458=CARTESIAN_POINT ( 'NONE',  ( -22.79553223295561892, 1.966428799096173075, -1.500000000000002220 ) ) ;
#13460=CARTESIAN_POINT ( 'NONE',  ( 21.36531308999010648, 3.172564587314818052, -1.500000000000002220 ) ) ;
#13461=CARTESIAN_POINT ( 'NONE',  ( -123.5204192411642339, -24.15543982623907482, -0.2315651400026561002 ) ) ;
#13462=CARTESIAN_POINT ( 'NONE',  ( -65.52287095715006160, -23.48783264082476308, -1.443836473390092578 ) ) ;
#13465=CARTESIAN_POINT ( 'NONE',  ( -1.797493081057526032, -22.44471576765463183, 11.49999999999999645 ) ) ;
#13466=VERTEX_POINT ( 'NONE', #84460 ) ;
#13467=CARTESIAN_POINT ( 'NONE',  ( -43.52287095715008292, -23.73907113217667586, -1.053371485781309680 ) ) ;
#13468=CARTESIAN_POINT ( 'NONE',  ( 20.22059317821533853, 8.664326447042464352, 11.49999999999998934 ) ) ;
#13470=CARTESIAN_POINT ( 'NONE',  ( -105.5960308574089623, -23.85049219812686871, 10.88485053497526955 ) ) ;
#13471=CARTESIAN_POINT ( 'NONE',  ( -28.66268959117890347, -24.79700224147869747, 7.176257715543974847 ) ) ;
#13473=EDGE_LOOP ( 'NONE', ( #56327, #57465, #34834, #28080 ) ) ;
#13475=CARTESIAN_POINT ( 'NONE',  ( -90.55338340485998572, -24.15602025860896163, 10.28564288303535434 ) ) ;
#13476=EDGE_LOOP ( 'NONE', ( #24794, #32677, #46905, #86541 ) ) ;
#13477=DIRECTION ( 'NONE',  ( -3.773278334444167608E-23, 1.000000000000000000, 0.000000000000000000 ) ) ;
#13478=ORIENTED_EDGE ( 'NONE', *, *, #37125, .T. ) ;
#13480=ORIENTED_EDGE ( 'NONE', *, *, #72614, .F. ) ;
#13482=LINE ( 'NONE', #90119, #53531 ) ;
#13485=CARTESIAN_POINT ( 'NONE',  ( 11.41020680648336771, 16.95828056793917682, -1.500000000000002220 ) ) ;
#13488=CARTESIAN_POINT ( 'NONE',  ( -99.52287095715006160, -23.48786465467241769, 11.44779295918254114 ) ) ;
#13490=CARTESIAN_POINT ( 'NONE',  ( -88.62287095715008434, -23.73934037231757443, 11.05740245334328797 ) ) ;
#13491=ORIENTED_EDGE ( 'NONE', *, *, #49916, .F. ) ;
#13492=CARTESIAN_POINT ( 'NONE',  ( -123.5228709571500474, -23.47593901973090524, -1.443836447538996204 ) ) ;
#13494=CARTESIAN_POINT ( 'NONE',  ( 20.60118427460899326, -2.865472796819775958, -1.500000000000002220 ) ) ;
#13496=CARTESIAN_POINT ( 'NONE',  ( -39.83231326723547028, -25.30536239359308226, 4.922453132992008484 ) ) ;
#13498=B_SPLINE_SURFACE_WITH_KNOTS ( 'NONE', 3, 3, ( 
 ( #81933, #64749, #97164, #27154 ),
 ( #41892, #19030, #33256, #71835 ),
 ( #2327, #3337, #80938, #11425 ),
 ( #66237, #65738, #64239, #80438 ),
 ( #50005, #11923, #95163, #56622 ),
 ( #4323, #18033, #73820, #49001 ),
 ( #10420, #26148, #10927, #57119 ) ),
 .UNSPECIFIED., .F., .F., .F.,
 ( 4, 3, 4 ),
 ( 4, 4 ),
 ( 0.7945040050992240310, 0.8970133687736498995, 0.9995227324480757680 ),
 ( 0.2895675803802711390, 0.2907139885458068229 ),
 .UNSPECIFIED. ) ;
#13500=ORIENTED_EDGE ( 'NONE', *, *, #35183, .T. ) ;
#13501=ORIENTED_EDGE ( 'NONE', *, *, #24696, .F. ) ;
#13503=CARTESIAN_POINT ( 'NONE',  ( -120.9228709571500104, -23.47593901973090524, -1.443836447538996426 ) ) ;
#13504=CARTESIAN_POINT ( 'NONE',  ( -55.52287095715005449, -23.48783264082477018, -1.443836473390094577 ) ) ;
#13505=CARTESIAN_POINT ( 'NONE',  ( -53.55620429048340014, -23.48783264082478084, -1.443836473390071040 ) ) ;
#13506=CARTESIAN_POINT ( 'NONE',  ( -5.843409716339609261, -21.38298466452703650, 11.49999999999999645 ) ) ;
#13507=VERTEX_POINT ( 'NONE', #53535 ) ;
#13510=CARTESIAN_POINT ( 'NONE',  ( -9.675873947287982446, 20.46574270456686406, 11.49999999999998934 ) ) ;
#13511=CARTESIAN_POINT ( 'NONE',  ( -99.60210373809772477, -25.30549553519965045, 4.950166919727378989 ) ) ;
#13515=ORIENTED_EDGE ( 'NONE', *, *, #63310, .T. ) ;
#13516=CARTESIAN_POINT ( 'NONE',  ( -69.55620429048339304, -23.47593901973091235, -1.443836447539006196 ) ) ;
#13517=EDGE_CURVE ( 'NONE', #78274, #53278, #45418, .T. ) ;
#13518=B_SPLINE_CURVE_WITH_KNOTS ( 'NONE', 3,
 ( #41120, #95892, #16758, #26387 ),
 .UNSPECIFIED., .F., .F.,
 ( 4, 4 ),
 ( 0.000000000000000000, 1.000000000000000000 ),
 .UNSPECIFIED. ) ;
#13519=CARTESIAN_POINT ( 'NONE',  ( -19.81368827760683260, -3.497637702615509880, -1.500000000000002220 ) ) ;
#13520=CARTESIAN_POINT ( 'NONE',  ( -57.64348235002147902, -23.96169478059713143, 10.65365249895718058 ) ) ;
#13522=CARTESIAN_POINT ( 'NONE',  ( -40.41373532093560073, -25.29345418465820572, 5.542204922786879706 ) ) ;
#13523=CARTESIAN_POINT ( 'NONE',  ( -21.31523168734759466, -6.469442287714795015, -1.500000000000002220 ) ) ;
#13524=VERTEX_POINT ( 'NONE', #98185 ) ;
#13526=CARTESIAN_POINT ( 'NONE',  ( -89.62287095715008434, -24.33927499327854704, 9.819080762295818943 ) ) ;
#13527=CARTESIAN_POINT ( 'NONE',  ( -26.02028971856659112, -24.71824093682183587, 2.619536031526803033 ) ) ;
#13529=CARTESIAN_POINT ( 'NONE',  ( -43.92287095715004597, -23.47596703998600276, 11.44779298504227683 ) ) ;
#13531=CARTESIAN_POINT ( 'NONE',  ( -7.634514033349506512, -17.95459398628807435, -1.500000000000002220 ) ) ;
#13532=CARTESIAN_POINT ( 'NONE',  ( -17.67684169981329845, 12.20363403927300183, 11.49999999999998934 ) ) ;
#13534=CARTESIAN_POINT ( 'NONE',  ( -110.5228709571500616, -29.50248789122583659, 2.256150453626215580 ) ) ;
#13535=FACE_OUTER_BOUND ( 'NONE', #48490, .T. ) ;
#13536=CARTESIAN_POINT ( 'NONE',  ( -21.14637036216210575, 8.611126525438130841, -1.500000000000002220 ) ) ;
#13537=ADVANCED_FACE ( 'NONE', ( #44925 ), #54032, .T. ) ;
#13538=EDGE_CURVE ( 'NONE', #66877, #89773, #46910, .T. ) ;
#13541=CARTESIAN_POINT ( 'NONE',  ( -96.54561769259652237, -24.66019654487199375, 8.947790411086115725 ) ) ;
#13542=CARTESIAN_POINT ( 'NONE',  ( -29.55620429048340725, -24.56818223648220112, 1.056161313644432997 ) ) ;
#13543=CARTESIAN_POINT ( 'NONE',  ( -18.20579941527595480, -8.200869797747142087, 11.49999999999999645 ) ) ;
#13544=LINE ( 'NONE', #44514, #38710 ) ;
#13546=CARTESIAN_POINT ( 'NONE',  ( -57.55620429048338593, -24.64898659630529210, 1.056161002820822814 ) ) ;
#13547=CARTESIAN_POINT ( 'NONE',  ( -46.62287095715004881, -29.50250786944525672, 11.44777988621624054 ) ) ;
#13549=CARTESIAN_POINT ( 'NONE',  ( -89.62287095715004170, -24.64898659630529210, 1.056161002820827921 ) ) ;
#13551=CARTESIAN_POINT ( 'NONE',  ( -21.53672441135761773, -2.854535511010750870, 11.49999999999998934 ) ) ;
#13554=CARTESIAN_POINT ( 'NONE',  ( -0.6043519431218743465, -19.59835197619436187, -1.500000000000002220 ) ) ;
#13556=CARTESIAN_POINT ( 'NONE',  ( -99.29844387660956784, -25.25464675839173978, 6.219202189682646598 ) ) ;
#13557=B_SPLINE_CURVE_WITH_KNOTS ( 'NONE', 3,
 ( #4690, #12280, #35640, #3205, #34146, #65112 ),
 .UNSPECIFIED., .F., .F.,
 ( 4, 2, 4 ),
 ( 6.384118678624473124E-06, 0.001386860460828385610, 0.002767336802978146663 ),
 .UNSPECIFIED. ) ;
#13558=ORIENTED_EDGE ( 'NONE', *, *, #95707, .T. ) ;
#13559=EDGE_CURVE ( 'NONE', #85635, #62904, #88083, .T. ) ;
#13562=CARTESIAN_POINT ( 'NONE',  ( -20.41219973434085944, 2.133827299322149429, 11.49999999999999645 ) ) ;
#13564=CARTESIAN_POINT ( 'NONE',  ( -113.6228709571500417, -24.66019654487199730, 8.947790411086121054 ) ) ;
#13566=CARTESIAN_POINT ( 'NONE',  ( -109.3584176993576591, -25.27948031066536672, 4.206202526585778756 ) ) ;
#13567=CARTESIAN_POINT ( 'NONE',  ( -39.81688933929658702, -25.18430914852639191, 3.494186188583478625 ) ) ;
#13569=EDGE_CURVE ( 'NONE', #95644, #24081, #23901, .T. ) ;
#13573=CARTESIAN_POINT ( 'NONE',  ( -100.6228709571500559, -24.99156045073393173, 7.747789690856161648 ) ) ;
#13574=CARTESIAN_POINT ( 'NONE',  ( 0.2859537766682072601, -23.01552763051285666, 11.49999999999999645 ) ) ;
#13575=CARTESIAN_POINT ( 'NONE',  ( 9.298244000614250382, 20.81247324795305431, 11.49999999999998934 ) ) ;
#13577=VECTOR ( 'NONE', #28211, 1000.000000000000114 ) ;
#13579=CARTESIAN_POINT ( 'NONE',  ( -120.5228709571500616, -24.82576562948882071, 8.398263436605679644 ) ) ;
#13580=CARTESIAN_POINT ( 'NONE',  ( -40.52287095715004028, -24.52323809116981579, 9.355190652339427260 ) ) ;
#13581=LINE ( 'NONE', #17089, #65969 ) ;
#13582=CARTESIAN_POINT ( 'NONE',  ( 6.492371748702247203, -20.92784845389783399, -1.500000000000002220 ) ) ;
#13583=EDGE_CURVE ( 'NONE', #55233, #90203, #78341, .T. ) ;
#13584=FACE_OUTER_BOUND ( 'NONE', #30868, .T. ) ;
#13585=CARTESIAN_POINT ( 'NONE',  ( -87.52215345038483463, -23.48786465467240703, 11.44779295918254647 ) ) ;
#13586=DIRECTION ( 'NONE',  ( -3.773278334444167608E-23, 1.000000000000000000, 0.000000000000000000 ) ) ;
#13587=EDGE_CURVE ( 'NONE', #75398, #18738, #29908, .T. ) ;
#13588=CARTESIAN_POINT ( 'NONE',  ( -28.62287095715004881, -29.50250243563660391, 8.947779535157950548 ) ) ;
#13590=CARTESIAN_POINT ( 'NONE',  ( -61.59189125704997281, -25.08279362854488781, 7.371166896404004909 ) ) ;
#13592=CARTESIAN_POINT ( 'NONE',  ( 19.37909195245082472, -6.530858791768283211, -1.500000000000002220 ) ) ;
#13593=ORIENTED_EDGE ( 'NONE', *, *, #83463, .F. ) ;
#13595=ORIENTED_EDGE ( 'NONE', *, *, #40219, .F. ) ;
#13596=ORIENTED_EDGE ( 'NONE', *, *, #47865, .F. ) ;
#13597=CARTESIAN_POINT ( 'NONE',  ( 19.24196208499951055, 12.69117723712289703, 11.49999999999998934 ) ) ;
#13598=CARTESIAN_POINT ( 'NONE',  ( -61.58760687538916301, -24.34968618360933945, 0.1864209137778810865 ) ) ;
#13599=EDGE_CURVE ( 'NONE', #91718, #95103, #93561, .T. ) ;
#13600=CARTESIAN_POINT ( 'NONE',  ( 13.55758662847591900, -15.04642845256218031, -1.500000000000002220 ) ) ;
#13601=ORIENTED_EDGE ( 'NONE', *, *, #5110, .F. ) ;
#13602=CARTESIAN_POINT ( 'NONE',  ( -29.96442039715612893, -23.42320092137126153, 11.44779298504228038 ) ) ;
#13605=CARTESIAN_POINT ( 'NONE',  ( -95.54583345656816107, -24.73486907724918282, 1.287355809206966128 ) ) ;
#13606=CARTESIAN_POINT ( 'NONE',  ( -70.57979237444475018, -24.92564183028979130, 1.928384488918253536 ) ) ;
#13607=CARTESIAN_POINT ( 'NONE',  ( -12.70309173801008562, -17.24390854791867511, 11.49999999999999645 ) ) ;
#13608=ORIENTED_EDGE ( 'NONE', *, *, #728, .T. ) ;
#13609=DIRECTION ( 'NONE',  ( 1.000000000000000000, 3.773278334444166432E-23, 8.201307841325785021E-29 ) ) ;
#13610=CARTESIAN_POINT ( 'NONE',  ( -41.48648435019234881, -24.51314013834315375, 0.6176544820404115121 ) ) ;
#13612=CARTESIAN_POINT ( 'NONE',  ( 18.79598114143782084, -8.675585332008726169, 11.49999999999998934 ) ) ;
#13614=LINE ( 'NONE', #53707, #16158 ) ;
#13615=VERTEX_POINT ( 'NONE', #227 ) ;
#13617=ORIENTED_EDGE ( 'NONE', *, *, #23902, .T. ) ;
#13618=CARTESIAN_POINT ( 'NONE',  ( -18.73635099073748833, 9.434554061794083069, -1.500000000000002220 ) ) ;
#13619=CARTESIAN_POINT ( 'NONE',  ( 3.689792033372774060, 21.67897595795444587, 11.49999999999999645 ) ) ;
#13620=CARTESIAN_POINT ( 'NONE',  ( -89.54348241549793386, -24.66019654487199730, 8.947790411086115725 ) ) ;
#13621=CARTESIAN_POINT ( 'NONE',  ( -22.39070119279581306, -2.479732019442284496, -1.500000000000002220 ) ) ;
#13622=CARTESIAN_POINT ( 'NONE',  ( 12.86141378215833342, 16.59024694808438127, -1.500000000000002220 ) ) ;
#13624=CARTESIAN_POINT ( 'NONE',  ( -72.62287095715005592, -23.72747288104442021, -1.053458166803662888 ) ) ;
#13625=CARTESIAN_POINT ( 'NONE',  ( -89.52287095715006160, -24.64898659630528854, 1.056161002820827921 ) ) ;
#13626=EDGE_CURVE ( 'NONE', #12687, #5012, #71002, .T. ) ;
#13627=EDGE_LOOP ( 'NONE', ( #3487, #42696, #1859, #44218 ) ) ;
#13630=CARTESIAN_POINT ( 'NONE',  ( -66.51029118470560775, -23.96119346886880308, -0.6495511937832151306 ) ) ;
#13632=B_SPLINE_CURVE_WITH_KNOTS ( 'NONE', 3,
 ( #58207, #81037, #26250, #34862 ),
 .UNSPECIFIED., .F., .F.,
 ( 4, 4 ),
 ( 0.000000000000000000, 9.999999999998897304E-05 ),
 .UNSPECIFIED. ) ;
#13633=CARTESIAN_POINT ( 'NONE',  ( -0.9917595143200197416, 21.46465604038169772, -1.500000000000002220 ) ) ;
#13634=EDGE_CURVE ( 'NONE', #40608, #89889, #52841, .T. ) ;
#13637=CARTESIAN_POINT ( 'NONE',  ( -19.39432879369159224, 8.380699159679657839, 11.49999999999998934 ) ) ;
#13639=CARTESIAN_POINT ( 'NONE',  ( -81.75072539166535535, -25.24685308744632195, 6.293942982122118224 ) ) ;
#13640=CARTESIAN_POINT ( 'NONE',  ( -83.63635015897777691, -23.96169478059713143, 10.65365249895718058 ) ) ;
#13642=CARTESIAN_POINT ( 'NONE',  ( 6.026614999332422182E-17, -23.47596703998571499, 11.44779284984881684 ) ) ;
#13643=CARTESIAN_POINT ( 'NONE',  ( -13.50798789833325664, 17.53495777034937220, -1.500000000000002220 ) ) ;
#13647=CARTESIAN_POINT ( 'NONE',  ( -64.58953762381672448, -23.47593901973091235, -1.443836447539007972 ) ) ;
#13648=CARTESIAN_POINT ( 'NONE',  ( -99.52287095715009002, -23.72773821059536914, 11.05748984161097503 ) ) ;
#13649=CARTESIAN_POINT ( 'NONE',  ( -100.5894454694905562, -24.52300882791526959, 0.6510814631126226049 ) ) ;
#13650=CARTESIAN_POINT ( 'NONE',  ( 11.34002819025610087, 15.78594478779102950, -1.500000000000002220 ) ) ;
#13651=CARTESIAN_POINT ( 'NONE',  ( -21.27170209485220198, -2.091907790468015005, -1.500000000000002220 ) ) ;
#13653=DIRECTION ( 'NONE',  ( -3.773278334444166432E-23, 1.000000000000000000, 0.000000000000000000 ) ) ;
#13654=CARTESIAN_POINT ( 'NONE',  ( -40.62287095715004170, -25.00158670708908204, 2.256160236439166411 ) ) ;
#13655=DIRECTION ( 'NONE',  ( -3.773278334453079030E-23, 0.9999999999976377785, 2.173523156925979128E-06 ) ) ;
#13656=CARTESIAN_POINT ( 'NONE',  ( -21.41681981171885951, -7.298096547245328303, -1.500000000000002220 ) ) ;
#13659=CARTESIAN_POINT ( 'NONE',  ( -108.6228709571500559, -29.50250243563736774, 8.947779886222136270 ) ) ;
#13661=CARTESIAN_POINT ( 'NONE',  ( -15.09475962229707591, 12.77647934908296712, 11.49999999999999645 ) ) ;
#13662=CARTESIAN_POINT ( 'NONE',  ( -59.62287095715005592, -23.73907113216990439, -1.053371485793229256 ) ) ;
#13663=CARTESIAN_POINT ( 'NONE',  ( -76.55620429048342146, -23.48783264082478084, -1.443836473390065933 ) ) ;
#13664=ORIENTED_EDGE ( 'NONE', *, *, #42415, .T. ) ;
#13665=CARTESIAN_POINT ( 'NONE',  ( -53.62287095715005592, -24.64965695001467694, 8.947790433994185832 ) ) ;
#13666=CARTESIAN_POINT ( 'NONE',  ( -68.52287095715003318, -23.96127896941631619, -0.6493128931038056884 ) ) ;
#13667=ADVANCED_FACE ( 'NONE', ( #46906 ), #63145, .F. ) ;
#13668=CARTESIAN_POINT ( 'NONE',  ( -0.6006773669993965559, 21.62980403441659760, -1.500000000000002220 ) ) ;
#13669=ADVANCED_FACE ( 'NONE', ( #32171 ), #79845, .T. ) ;
#13670=CARTESIAN_POINT ( 'NONE',  ( -26.49193215146072689, -24.84431178523845674, 6.877568485563839040 ) ) ;
#13671=CARTESIAN_POINT ( 'NONE',  ( 6.036767712469883307, 18.47306877840545170, -1.500000000000002220 ) ) ;
#13672=B_SPLINE_CURVE_WITH_KNOTS ( 'NONE', 3,
 ( #70145, #30581, #84365, #21951, #8250, #46819, #52936, #15347, #31579, #631, #77735, #46310 ),
 .UNSPECIFIED., .F., .F.,
 ( 4, 2, 2, 2, 2, 4 ),
 ( 0.000000000000000000, 0.0001663275863830617580, 0.0003326551727661235160, 0.0006653103455322287091, 0.0009979655182983339021, 0.001330620691064439204 ),
 .UNSPECIFIED. ) ;
#13674=CARTESIAN_POINT ( 'NONE',  ( -82.52287095715003318, -23.73934037231756022, 11.05740245334328620 ) ) ;
#13675=CARTESIAN_POINT ( 'NONE',  ( -93.52287095715006160, -23.48786465467241769, 11.44779295918254292 ) ) ;
#13676=CARTESIAN_POINT ( 'NONE',  ( 19.71268880909926580, -1.816447362451163450, -1.500000000000002220 ) ) ;
#13678=EDGE_CURVE ( 'NONE', #94726, #100015, #39544, .T. ) ;
#13679=B_SPLINE_CURVE_WITH_KNOTS ( 'NONE', 3,
 ( #1692, #63604, #78786, #32627 ),
 .UNSPECIFIED., .F., .F.,
 ( 4, 4 ),
 ( 0.000000000000000000, 9.999999999998897304E-05 ),
 .UNSPECIFIED. ) ;
#13681=CARTESIAN_POINT ( 'NONE',  ( 17.44645523915803764, -10.38078700900905993, 11.49999999999999645 ) ) ;
#13682=DIRECTION ( 'NONE',  ( -0.000000000000000000, 2.173523156925979552E-06, -0.9999999999976378895 ) ) ;
#13683=CARTESIAN_POINT ( 'NONE',  ( -105.6228709571500417, -24.99132157543166954, 2.256160258750667502 ) ) ;
#13684=EDGE_LOOP ( 'NONE', ( #70318, #99707, #23860, #75491 ) ) ;
#13685=B_SPLINE_SURFACE_WITH_KNOTS ( 'NONE', 3, 3, ( 
 ( #13096, #74996, #22699, #5995 ),
 ( #29332, #99335, #14601, #53686 ),
 ( #52177, #12608, #44566, #5497 ),
 ( #22202, #20711, #6502, #6997 ),
 ( #37452, #13598, #37944, #5001 ),
 ( #28839, #97839, #90738, #36446 ),
 ( #30326, #68403, #66919, #28333 ) ),
 .UNSPECIFIED., .F., .F., .F.,
 ( 4, 3, 4 ),
 ( 4, 4 ),
 ( 0.0004766839783815518170, 0.1029713700210893451, 0.2054660560637971423 ),
 ( 0.6896694373704013170, 0.6910003741376167241 ),
 .UNSPECIFIED. ) ;
#13686=CARTESIAN_POINT ( 'NONE',  ( -102.6362921444641501, -23.48786465467241058, 11.44779295918254292 ) ) ;
#13690=CARTESIAN_POINT ( 'NONE',  ( -123.6228709571500559, -29.50247984919015209, -1.443849546365046699 ) ) ;
#13691=CARTESIAN_POINT ( 'NONE',  ( 1.781536345648733199, 20.00535218256611358, 11.49999999999998934 ) ) ;
#13692=EDGE_CURVE ( 'NONE', #13741, #43203, #72254, .T. ) ;
#13693=EDGE_CURVE ( 'NONE', #64178, #75014, #58965, .T. ) ;
#13694=CARTESIAN_POINT ( 'NONE',  ( -28.52287095715007226, -23.32374950011072912, -1.443835813551990643 ) ) ;
#13696=CARTESIAN_POINT ( 'NONE',  ( -117.6228709571500133, -23.95044443724991368, 10.65354141964649592 ) ) ;
#13697=CARTESIAN_POINT ( 'NONE',  ( 17.53461989915211916, -14.66684187699354425, 11.49999999999999645 ) ) ;
#13698=CARTESIAN_POINT ( 'NONE',  ( -49.50841769935764347, -25.31297054157952431, 3.984447646101154650 ) ) ;
#13699=CARTESIAN_POINT ( 'NONE',  ( -82.58953762381671027, -24.65952944569304606, 1.056160979905701902 ) ) ;
#13700=CARTESIAN_POINT ( 'NONE',  ( -53.52287095715008292, -23.47593901973090169, -1.443836447538997092 ) ) ;
#13702=AXIS2_PLACEMENT_3D ( 'NONE', #26453, #48289, #2619 ) ;
#13703=ADVANCED_FACE ( 'NONE', ( #18453 ), #34685, .T. ) ;
#13704=CARTESIAN_POINT ( 'NONE',  ( -32.52287095715004739, -23.47593901973090169, -1.443836447538997092 ) ) ;
#13705=B_SPLINE_CURVE_WITH_KNOTS ( 'NONE', 3,
 ( #4651, #89381, #19852, #50828, #43220, #66576 ),
 .UNSPECIFIED., .F., .F.,
 ( 4, 2, 4 ),
 ( 1.570887131794952276E-05, 0.001396322306279764325, 0.002776935741241578874 ),
 .UNSPECIFIED. ) ;
#13706=CARTESIAN_POINT ( 'NONE',  ( -99.62287095715005592, -29.50247984919015209, -1.443849546365050029 ) ) ;
#13707=ORIENTED_EDGE ( 'NONE', *, *, #49923, .F. ) ;
#13708=CARTESIAN_POINT ( 'NONE',  ( -14.79517943714664518, -13.99575967537150412, 11.49999999999998934 ) ) ;
#13710=CARTESIAN_POINT ( 'NONE',  ( -6.529369910325518944, -22.02198592821369516, -1.500000000000002220 ) ) ;
#13712=CARTESIAN_POINT ( 'NONE',  ( -115.5895376238167245, -23.48786465467242479, 11.44779295918253759 ) ) ;
#13715=CARTESIAN_POINT ( 'NONE',  ( -108.6247740409122571, -24.51419770103158768, 9.386484678747162747 ) ) ;
#13717=CARTESIAN_POINT ( 'NONE',  ( -67.52287095715001897, -23.95044443724991723, 10.65354141964649415 ) ) ;
#13720=CARTESIAN_POINT ( 'NONE',  ( -12.29646723538143505, -17.35194501319736560, 11.49999999999999645 ) ) ;
#13721=EDGE_LOOP ( 'NONE', ( #92403, #5993, #25233, #30946 ) ) ;
#13723=CARTESIAN_POINT ( 'NONE',  ( 12.08182546098005972, -18.57710416600862402, -1.500000000000002220 ) ) ;
#13724=CARTESIAN_POINT ( 'NONE',  ( 1.647368763193059582, 20.57021071130147405, -1.500000000000002220 ) ) ;
#13726=ORIENTED_EDGE ( 'NONE', *, *, #19667, .T. ) ;
#13728=CARTESIAN_POINT ( 'NONE',  ( -39.04303308397305727, -25.29008967749855685, 4.215216926603018166 ) ) ;
#13730=VERTEX_POINT ( 'NONE', #4233 ) ;
#13732=CARTESIAN_POINT ( 'NONE',  ( -41.49885461251451346, -24.15620529776627734, 10.23563542870660825 ) ) ;
#13733=DIRECTION ( 'NONE',  ( 0.000000000000000000, -0.9999999999976377785, -2.173523156925979128E-06 ) ) ;
#13734=CARTESIAN_POINT ( 'NONE',  ( -8.730572200882948053, 18.91488879456464289, -1.500000000000002220 ) ) ;
#13735=CARTESIAN_POINT ( 'NONE',  ( -19.76859095128058996, -9.124614402804876789, 11.49999999999999645 ) ) ;
#13736=CARTESIAN_POINT ( 'NONE',  ( -50.88733314876014902, -25.04353333182355357, 7.513223449029553080 ) ) ;
#13737=CARTESIAN_POINT ( 'NONE',  ( -77.52287095715006160, -23.48786465467241058, 11.44779295918254469 ) ) ;
#13738=CARTESIAN_POINT ( 'NONE',  ( -115.5149161931255719, -24.73486907724918282, 1.287355809206964352 ) ) ;
#13739=CARTESIAN_POINT ( 'NONE',  ( -16.84940295534276800, 14.81145437567392698, 11.49999999999998934 ) ) ;
#13740=CARTESIAN_POINT ( 'NONE',  ( -51.22891850606554698, -25.31296662437967626, 4.264007001526691987 ) ) ;
#13741=VERTEX_POINT ( 'NONE', #26576 ) ;
#13746=B_SPLINE_CURVE_WITH_KNOTS ( 'NONE', 3,
 ( #64316, #64822, #95735, #26224, #88131, #18599, #97727, #19598, #42960, #44450, #91109, #20100, #28722, #29216 ),
 .UNSPECIFIED., .F., .F.,
 ( 4, 2, 2, 2, 2, 2, 4 ),
 ( 2.809234570782672869E-17, 0.0001998554611590488311, 0.0003997109223180695813, 0.0007994218446360915661, 0.001199132766954113605, 0.001398988228113124625, 0.001598843689272135644 ),
 .UNSPECIFIED. ) ;
#13747=ORIENTED_EDGE ( 'NONE', *, *, #61912, .T. ) ;
#13748=DIRECTION ( 'NONE',  ( -3.773278334444166432E-23, 1.000000000000000000, 0.000000000000000000 ) ) ;
#13749=ORIENTED_EDGE ( 'NONE', *, *, #50593, .T. ) ;
#13750=CARTESIAN_POINT ( 'NONE',  ( -21.26230640008892792, -0.7210608269398429693, -1.500000000000002220 ) ) ;
#13751=VERTEX_POINT ( 'NONE', #11344 ) ;
#13753=CARTESIAN_POINT ( 'NONE',  ( 7.388015978253313243, 19.69965359013245632, -1.500000000000002220 ) ) ;
#13754=CARTESIAN_POINT ( 'NONE',  ( -35.52287095715006870, -25.00158670708909270, 2.256160236439166411 ) ) ;
#13755=CARTESIAN_POINT ( 'NONE',  ( -110.8642813400260678, -25.21264688230269968, 3.422668213661852032 ) ) ;
#13757=CARTESIAN_POINT ( 'NONE',  ( -21.49438740719132923, 4.340694165963498996, -1.500000000000002220 ) ) ;
#13761=CARTESIAN_POINT ( 'NONE',  ( -84.58277711012007671, -24.66019654487200441, 8.947790411086119278 ) ) ;
#13762=B_SPLINE_CURVE_WITH_KNOTS ( 'NONE', 3,
 ( #82408, #5287, #36248, #68192 ),
 .UNSPECIFIED., .F., .F.,
 ( 4, 4 ),
 ( 1.387778780781445676E-17, 0.0001000000000000028508 ),
 .UNSPECIFIED. ) ;
#13763=LINE ( 'NONE', #61468, #95971 ) ;
#13764=DIRECTION ( 'NONE',  ( 0.000000000000000000, -0.9999999999976377785, -2.173523156925979975E-06 ) ) ;
#13765=CARTESIAN_POINT ( 'NONE',  ( 21.14028111218437900, -2.610574537768086234, 11.49999999999998934 ) ) ;
#13767=CARTESIAN_POINT ( 'NONE',  ( -107.5907561945975459, -24.15620529776628800, 10.23563542870659759 ) ) ;
#13768=AXIS2_PLACEMENT_3D ( 'NONE', #16089, #86106, #47560 ) ;
#13769=CARTESIAN_POINT ( 'NONE',  ( -29.52287095715006160, -23.38909342368989641, 11.44779306042727285 ) ) ;
#13770=CARTESIAN_POINT ( 'NONE',  ( -33.65849158002127695, -23.73766607897670866, -1.055555164236444909 ) ) ;
#13771=CARTESIAN_POINT ( 'NONE',  ( -19.72384299526936857, -10.77339039931002773, -1.500000000000002220 ) ) ;
#13772=CARTESIAN_POINT ( 'NONE',  ( -110.3139465455115129, -29.50248914370730091, 2.832395270851967073 ) ) ;
#13773=ORIENTED_EDGE ( 'NONE', *, *, #23318, .F. ) ;
#13774=ADVANCED_FACE ( 'NONE', ( #97571 ), #81852, .F. ) ;
#13775=CARTESIAN_POINT ( 'NONE',  ( -98.89303308397306580, -25.26498937201382233, 6.110950154240443410 ) ) ;
#13776=CARTESIAN_POINT ( 'NONE',  ( -2.340448316220725467, 19.49152957720520618, 11.49999999999999645 ) ) ;
#13777=LINE ( 'NONE', #82799, #29265 ) ;
#13778=ADVANCED_FACE ( 'NONE', ( #19942 ), #3252, .F. ) ;
#13783=CARTESIAN_POINT ( 'NONE',  ( -69.60169030842801874, -25.30567014228302725, 5.021178964433338443 ) ) ;
#13784=CARTESIAN_POINT ( 'NONE',  ( -99.33274021282838362, -25.31439685940647877, 5.901068652850602447 ) ) ;
#13785=EDGE_CURVE ( 'NONE', #32994, #83380, #79423, .T. ) ;
#13786=AXIS2_PLACEMENT_3D ( 'NONE', #4388, #18103, #34335 ) ;
#13787=CARTESIAN_POINT ( 'NONE',  ( -122.5228709571500758, -23.47593901973090524, -1.443836447538996204 ) ) ;
#13788=EDGE_CURVE ( 'NONE', #26222, #19840, #12932, .T. ) ;
#13789=CARTESIAN_POINT ( 'NONE',  ( -2.117704968268854682, 19.61795684621070990, 11.49999999999998934 ) ) ;
#13792=CARTESIAN_POINT ( 'NONE',  ( -70.62287095715004170, -23.48783264082478084, -1.443836473390067265 ) ) ;
#13795=ORIENTED_EDGE ( 'NONE', *, *, #98031, .F. ) ;
#13796=CARTESIAN_POINT ( 'NONE',  ( -124.5228709571500616, -24.64965694238575722, 8.947790433994191162 ) ) ;
#13798=CARTESIAN_POINT ( 'NONE',  ( -55.49176352103356180, -24.52300882791530157, 0.6510814631126364826 ) ) ;
#13799=CARTESIAN_POINT ( 'NONE',  ( -118.5566399227117245, -23.73766607897671221, -1.055555164236448462 ) ) ;
#13801=CARTESIAN_POINT ( 'NONE',  ( -99.62287095715016960, -24.35013146730204170, 9.818937971375104823 ) ) ;
#13802=FACE_OUTER_BOUND ( 'NONE', #85470, .T. ) ;
#13803=CARTESIAN_POINT ( 'NONE',  ( 18.25133680241413359, 8.160682379734268466, -1.500000000000002220 ) ) ;
#13805=DIRECTION ( 'NONE',  ( -3.773278334453080206E-23, 0.9999999999976377785, 2.173523156925979552E-06 ) ) ;
#13806=CARTESIAN_POINT ( 'NONE',  ( -45.47735399304787052, -24.83644354573577928, 8.397322867130094792 ) ) ;
#13808=CARTESIAN_POINT ( 'NONE',  ( -74.58953762381673869, -24.64898659630367561, 1.056161002820383388 ) ) ;
#13810=EDGE_CURVE ( 'NONE', #34688, #26860, #60028, .T. ) ;
#13811=CARTESIAN_POINT ( 'NONE',  ( -119.5202043240208383, -23.96119346886881019, -0.6495511937832018079 ) ) ;
#13814=CARTESIAN_POINT ( 'NONE',  ( -126.8947205558307303, -25.24722654741731276, 6.200372419592135920 ) ) ;
#13815=CARTESIAN_POINT ( 'NONE',  ( -81.59989050339841299, -23.73766607897671221, -1.055555164236432919 ) ) ;
#13817=CARTESIAN_POINT ( 'NONE',  ( -51.69567503897438598, -25.26279930336529489, 4.127965216627219824 ) ) ;
#13818=B_SPLINE_CURVE_WITH_KNOTS ( 'NONE', 3,
 ( #37867, #31244, #68817, #23116 ),
 .UNSPECIFIED., .F., .F.,
 ( 4, 4 ),
 ( 0.1706218368772978167, 0.1796282681494135169 ),
 .UNSPECIFIED. ) ;
#13819=B_SPLINE_CURVE_WITH_KNOTS ( 'NONE', 3,
 ( #17240, #63954, #25855, #40086 ),
 .UNSPECIFIED., .F., .F.,
 ( 4, 4 ),
 ( 2.775557561562891351E-17, 9.999999999996123101E-05 ),
 .UNSPECIFIED. ) ;
#13820=CARTESIAN_POINT ( 'NONE',  ( -87.62287095715004170, -24.65952944569304606, 1.056160979905700348 ) ) ;
#13821=CARTESIAN_POINT ( 'NONE',  ( -127.5898613667035875, -24.15543982623907837, -0.2315651400026538520 ) ) ;
#13823=CARTESIAN_POINT ( 'NONE',  ( -12.33117494125061242, 16.09929768045241261, -1.500000000000002220 ) ) ;
#13824=B_SPLINE_CURVE_WITH_KNOTS ( 'NONE', 3,
 ( #92998, #99111, #22973, #99602, #38718, #54454 ),
 .UNSPECIFIED., .F., .F.,
 ( 4, 2, 4 ),
 ( 0.000000000000000000, 0.001380764517854760629, 0.002761529035709521258 ),
 .UNSPECIFIED. ) ;
#13825=CARTESIAN_POINT ( 'NONE',  ( -122.6250502620820981, -24.15543982623907482, -0.2315651400026565443 ) ) ;
#13826=CARTESIAN_POINT ( 'NONE',  ( -116.6228709571500559, -29.50247984919015209, -1.443849546365046699 ) ) ;
#13827=CARTESIAN_POINT ( 'NONE',  ( -34.52287095715006160, -23.47596703998600631, 11.44779298504229459 ) ) ;
#13828=EDGE_CURVE ( 'NONE', #40606, #66289, #8091, .T. ) ;
#13829=EDGE_LOOP ( 'NONE', ( #37355, #27458, #22741, #77854 ) ) ;
#13831=PLANE ( 'NONE',  #77775 ) ;
#13832=CARTESIAN_POINT ( 'NONE',  ( -18.22032804147677254, 8.545885342870345625, -1.500000000000002220 ) ) ;
#13833=CARTESIAN_POINT ( 'NONE',  ( 12.48895993392301307, -16.95307763291877379, 11.49999999999999645 ) ) ;
#13835=CARTESIAN_POINT ( 'NONE',  ( -70.53621709966942888, -24.83644354573578283, 8.397322867130098345 ) ) ;
#13836=CARTESIAN_POINT ( 'NONE',  ( -13.14421341422731260, -17.72855101262432242, 11.49999999999998934 ) ) ;
#13837=EDGE_CURVE ( 'NONE', #16488, #84333, #3256, .T. ) ;
#13839=CARTESIAN_POINT ( 'NONE',  ( 2.947869850540926429, 20.32360706268488215, -1.500000000000002220 ) ) ;
#13840=CARTESIAN_POINT ( 'NONE',  ( -66.52287095715003318, -24.66019654487199375, 8.947790411086119278 ) ) ;
#13842=CARTESIAN_POINT ( 'NONE',  ( -59.58953762381671737, -24.64898659630367916, 1.056161002820383166 ) ) ;
#13843=ORIENTED_EDGE ( 'NONE', *, *, #10142, .F. ) ;
#13846=DIRECTION ( 'NONE',  ( -3.773278334453079618E-23, 0.9999999999976377785, 2.173523156925979975E-06 ) ) ;
#13847=CARTESIAN_POINT ( 'NONE',  ( -72.52287095715007581, -24.64965694238575011, 8.947790433994200043 ) ) ;
#13848=VERTEX_POINT ( 'NONE', #51406 ) ;
#13850=ORIENTED_EDGE ( 'NONE', *, *, #22985, .T. ) ;
#13853=CARTESIAN_POINT ( 'NONE',  ( -76.58157264639545758, -24.65952944569303895, 1.056160979905700792 ) ) ;
#13854=CARTESIAN_POINT ( 'NONE',  ( 0.1292827521129817636, -20.55975067039486603, -1.500000000000002220 ) ) ;
#13855=B_SPLINE_CURVE_WITH_KNOTS ( 'NONE', 3,
 ( #79749, #80257, #35089, #86857 ),
 .UNSPECIFIED., .F., .F.,
 ( 4, 4 ),
 ( 0.9311649220781571534, 0.9401713533502727982 ),
 .UNSPECIFIED. ) ;
#13857=CARTESIAN_POINT ( 'NONE',  ( -8.750087785235610482, 19.73178376063210138, 11.49999999999999645 ) ) ;
#13859=DIRECTION ( 'NONE',  ( -1.000000000000000000, -3.773278334444167608E-23, -8.201307833595939069E-29 ) ) ;
#13860=CARTESIAN_POINT ( 'NONE',  ( -35.55620429048339304, -23.48783264082477729, -1.443836473390072372 ) ) ;
#13861=CARTESIAN_POINT ( 'NONE',  ( 18.00092565640838416, -13.26076702590692769, 11.49999999999998934 ) ) ;
#13862=VECTOR ( 'NONE', #47810, 1000.000000000000114 ) ;
#13863=CARTESIAN_POINT ( 'NONE',  ( -117.5228709571500332, -24.66019654487200441, 8.947790411086108620 ) ) ;
#13864=CARTESIAN_POINT ( 'NONE',  ( -84.55446260568123762, -23.96119346886880663, -0.6495511937832096905 ) ) ;
#13867=DIRECTION ( 'NONE',  ( -3.773278334453079030E-23, 0.9999999999976377785, 2.173523156925979128E-06 ) ) ;
#13868=CARTESIAN_POINT ( 'NONE',  ( 20.83135763335140922, 1.668377004047274959, 11.49999999999998934 ) ) ;
#13870=CARTESIAN_POINT ( 'NONE',  ( -67.49690699276101213, -24.51419770103159124, 9.386484678747168076 ) ) ;
#13871=ORIENTED_EDGE ( 'NONE', *, *, #45884, .T. ) ;
#13872=ORIENTED_EDGE ( 'NONE', *, *, #3410, .T. ) ;
#13873=CARTESIAN_POINT ( 'NONE',  ( -100.6291315273262796, -24.52399227489127398, 9.353111116836521077 ) ) ;
#13874=CARTESIAN_POINT ( 'NONE',  ( -19.39432879369159224, 8.380699159679657839, -1.500000000000002220 ) ) ;
#13875=ORIENTED_EDGE ( 'NONE', *, *, #54270, .F. ) ;
#13876=CARTESIAN_POINT ( 'NONE',  ( -117.6294079147639593, -23.48783264082477018, -1.443836473390081254 ) ) ;
#13878=CARTESIAN_POINT ( 'NONE',  ( -0.2038501785326352067, 21.78777694363981254, -1.500000000000002220 ) ) ;
#13879=CARTESIAN_POINT ( 'NONE',  ( -76.51686106428668666, -23.73791477778911840, 11.05961554403170766 ) ) ;
#13881=CARTESIAN_POINT ( 'NONE',  ( 14.05712878599199200, -16.60762996970646199, -1.500000000000002220 ) ) ;
#13882=CARTESIAN_POINT ( 'NONE',  ( -71.60837349177994327, -25.31639633020554925, 5.637668385895925560 ) ) ;
#13883=CARTESIAN_POINT ( 'NONE',  ( -0.4079105510268487000, 22.33655531192813370, 11.49999999999999645 ) ) ;
#13884=ORIENTED_EDGE ( 'NONE', *, *, #82442, .F. ) ;
#13885=CARTESIAN_POINT ( 'NONE',  ( -31.24388727629348494, -29.50248678627064081, 1.747779886239157809 ) ) ;
#13886=CARTESIAN_POINT ( 'NONE',  ( -123.5562042904833930, -24.65952944569304961, 1.056160979905707453 ) ) ;
#13888=ORIENTED_EDGE ( 'NONE', *, *, #58258, .T. ) ;
#13892=CARTESIAN_POINT ( 'NONE',  ( -20.47705334459678994, -22.77463087841388045, -1.497999999999533038 ) ) ;
#13893=CARTESIAN_POINT ( 'NONE',  ( -34.62287095715005592, -23.48786465467240347, 11.44779295918255535 ) ) ;
#13895=CARTESIAN_POINT ( 'NONE',  ( -75.62287095715004170, -24.99132157543084176, 2.256160258750667502 ) ) ;
#13897=CARTESIAN_POINT ( 'NONE',  ( 2.021814659504407579E-13, -19.30000000000000426, -1.500000000000002220 ) ) ;
#13898=ADVANCED_FACE ( 'NONE', ( #44794 ), #89961, .F. ) ;
#13899=CARTESIAN_POINT ( 'NONE',  ( -36.58953762381673158, -24.66019654487199375, 8.947790411086137041 ) ) ;
#13902=CARTESIAN_POINT ( 'NONE',  ( 9.746180923669104601, -16.83516941858706417, 11.49999999999999645 ) ) ;
#13903=CARTESIAN_POINT ( 'NONE',  ( -87.62287095715004170, -23.47596703998600631, 11.44779298504227860 ) ) ;
#13904=VERTEX_POINT ( 'NONE', #45784 ) ;
#13907=FACE_OUTER_BOUND ( 'NONE', #39491, .T. ) ;
#13908=FACE_OUTER_BOUND ( 'NONE', #99616, .T. ) ;
#13910=CARTESIAN_POINT ( 'NONE',  ( -121.2228709571500644, -23.47596703998600631, 11.44779298504227860 ) ) ;
#13911=CARTESIAN_POINT ( 'NONE',  ( -16.92291128558595048, 9.936001969431544012, -1.500000000000002220 ) ) ;
#13912=EDGE_CURVE ( 'NONE', #11900, #31349, #98056, .T. ) ;
#13915=CARTESIAN_POINT ( 'NONE',  ( -5.754811884962036217, -20.78327508566754389, -1.500000000000002220 ) ) ;
#13918=CARTESIAN_POINT ( 'NONE',  ( -70.70074709382635092, -25.12219130706001735, 7.037036740594547091 ) ) ;
#13919=CARTESIAN_POINT ( 'NONE',  ( -50.52287095715006160, -24.99132157543166599, 2.256160258750667502 ) ) ;
#13920=CARTESIAN_POINT ( 'NONE',  ( -99.78454658038423020, -25.18439381177101311, 3.502964603859448633 ) ) ;
#13921=CARTESIAN_POINT ( 'NONE',  ( 17.08057647167376913, 15.47633299359885761, -1.500000000000002220 ) ) ;
#13924=LINE ( 'NONE', #73840, #51523 ) ;
#13925=CARTESIAN_POINT ( 'NONE',  ( -49.48969932074964362, -24.51314013834316086, 0.6176544820404130665 ) ) ;
#13926=CARTESIAN_POINT ( 'NONE',  ( -20.08517628505838815, -1.856936949192496300, 11.49999999999999645 ) ) ;
#13927=CARTESIAN_POINT ( 'NONE',  ( -109.1001591083545179, -25.10927551888114806, 3.548369107942201062 ) ) ;
#13931=CARTESIAN_POINT ( 'NONE',  ( -46.52287095715004028, -24.34917612406836795, 0.1852690917426517980 ) ) ;
#13933=CARTESIAN_POINT ( 'NONE',  ( -38.62287095715005592, -24.64898659630528144, 1.056161002820819261 ) ) ;
#13934=CARTESIAN_POINT ( 'NONE',  ( -0.2410636032128395945, 19.88167143085883737, -1.500000000000002220 ) ) ;
#13936=CARTESIAN_POINT ( 'NONE',  ( -109.5562042904834072, -24.64898659630530275, 1.056161002820833472 ) ) ;
#13937=CARTESIAN_POINT ( 'NONE',  ( 5.037983044326730386, -19.10262670698400100, -1.500000000000002220 ) ) ;
#13939=CARTESIAN_POINT ( 'NONE',  ( -126.6237056494491924, -24.51419770103158413, 9.386484678747162747 ) ) ;
#13940=CARTESIAN_POINT ( 'NONE',  ( -110.5228709571499763, -24.82576562948881715, 8.398263436605676091 ) ) ;
#13942=CARTESIAN_POINT ( 'NONE',  ( 15.29587703590233971, -13.95322596517325664, 11.49999999999999645 ) ) ;
#13945=CARTESIAN_POINT ( 'NONE',  ( -106.5947035255675814, -23.73766607897671577, -1.055555164236449572 ) ) ;
#13946=CARTESIAN_POINT ( 'NONE',  ( -1.179572987637725889, 22.66035800735570049, 11.49999999999999645 ) ) ;
#13948=CARTESIAN_POINT ( 'NONE',  ( -91.62287095715005592, -23.72747288104469376, -1.053458166803225682 ) ) ;
#13950=CARTESIAN_POINT ( 'NONE',  ( 9.409760114191467295, 17.86087837679851020, -1.500000000000002220 ) ) ;
#13952=CARTESIAN_POINT ( 'NONE',  ( -106.5228709571500758, -29.50250786944525672, 11.44777988621622988 ) ) ;
#13954=VERTEX_POINT ( 'NONE', #13820 ) ;
#13955=B_SPLINE_CURVE_WITH_KNOTS ( 'NONE', 3,
 ( #22583, #29723, #84999, #53075, #21593, #15483 ),
 .UNSPECIFIED., .F., .F.,
 ( 4, 2, 4 ),
 ( 0.000000000000000000, 0.001380764517854765616, 0.002761529035709531232 ),
 .UNSPECIFIED. ) ;
#13958=CARTESIAN_POINT ( 'NONE',  ( 21.91704834537361180, 6.644925864936762849, -1.500000000000002220 ) ) ;
#13959=CARTESIAN_POINT ( 'NONE',  ( -29.57433297125452754, -24.58015684836148296, 1.056161296257513982 ) ) ;
#13960=CARTESIAN_POINT ( 'NONE',  ( -20.99440926880444636, 4.982473936180791263, -1.500000000000002220 ) ) ;
#13961=CARTESIAN_POINT ( 'NONE',  ( -123.5552300364399798, -24.15543982623907482, -0.2315651400026561002 ) ) ;
#13963=CARTESIAN_POINT ( 'NONE',  ( 12.60132613692001691, 16.66296579206088069, 11.49999999999999645 ) ) ;
#13964=ORIENTED_EDGE ( 'NONE', *, *, #84526, .T. ) ;
#13965=CARTESIAN_POINT ( 'NONE',  ( -28.87341653796864804, -25.01351064681628245, 2.972253445286453744 ) ) ;
#13966=CARTESIAN_POINT ( 'NONE',  ( 13.70243205411677145, -17.22335469805116048, -1.500000000000002220 ) ) ;
#13969=CARTESIAN_POINT ( 'NONE',  ( -41.77018777319382536, -25.10925950928115569, 3.672890040647070808 ) ) ;
#13970=ORIENTED_EDGE ( 'NONE', *, *, #59755, .F. ) ;
#13971=FACE_OUTER_BOUND ( 'NONE', #2192, .T. ) ;
#13974=ORIENTED_EDGE ( 'NONE', *, *, #5101, .F. ) ;
#13975=CARTESIAN_POINT ( 'NONE',  ( -72.49891841213921850, -24.51419770103156281, 9.386484678747185839 ) ) ;
#13976=ORIENTED_EDGE ( 'NONE', *, *, #21050, .T. ) ;
#13980=CARTESIAN_POINT ( 'NONE',  ( -57.59852009964687625, -23.96119346886880663, -0.6495511937832122440 ) ) ;
#13981=CARTESIAN_POINT ( 'NONE',  ( 7.100489274569507181, 19.11111018586187527, -1.500000000000002220 ) ) ;
#13984=CARTESIAN_POINT ( 'NONE',  ( -30.59800378598952264, -24.75991027412949563, 1.063373454495736725 ) ) ;
#13986=CARTESIAN_POINT ( 'NONE',  ( -25.57847374984697097, -24.89029040080884414, 5.862545262149446934 ) ) ;
#13988=CARTESIAN_POINT ( 'NONE',  ( -99.62287095715005592, -23.47596703998600631, 11.44779298504227860 ) ) ;
#13989=CARTESIAN_POINT ( 'NONE',  ( -29.39543059329891506, -25.26247846418970866, 7.191771738233368794 ) ) ;
#13990=CARTESIAN_POINT ( 'NONE',  ( 19.16185898538474675, 8.078635803559651052, -1.500000000000002220 ) ) ;
#13993=VERTEX_POINT ( 'NONE', #43795 ) ;
#13995=CARTESIAN_POINT ( 'NONE',  ( -104.6228709571500559, -29.50247984919015209, -1.443849546365050029 ) ) ;
#13996=EDGE_LOOP ( 'NONE', ( #40507, #96436, #98762, #31077 ) ) ;
#13997=ORIENTED_EDGE ( 'NONE', *, *, #53233, .T. ) ;
#14001=DIRECTION ( 'NONE',  ( 0.000000000000000000, -0.9999999999976377785, -2.173523156925979975E-06 ) ) ;
#14003=CARTESIAN_POINT ( 'NONE',  ( -80.58953762381673869, -25.00158670708909270, 2.256160236439166411 ) ) ;
#14004=CARTESIAN_POINT ( 'NONE',  ( -92.60130859751525634, -23.48786465467241058, 11.44779295918254469 ) ) ;
#14006=CARTESIAN_POINT ( 'NONE',  ( 2.710298230372018669, -21.94706154713207980, 11.49999999999999645 ) ) ;
#14008=PLANE ( 'NONE',  #71611 ) ;
#14009=CARTESIAN_POINT ( 'NONE',  ( -22.43363504178351775, 2.973318333978472339, -1.500000000000002220 ) ) ;
#14010=AXIS2_PLACEMENT_3D ( 'NONE', #8586, #17191, #15692 ) ;
#14011=CARTESIAN_POINT ( 'NONE',  ( -28.70162415927573818, -24.97191045107068064, 7.134260916763030203 ) ) ;
#14012=ORIENTED_EDGE ( 'NONE', *, *, #87134, .T. ) ;
#14013=ORIENTED_EDGE ( 'NONE', *, *, #75886, .F. ) ;
#14015=CARTESIAN_POINT ( 'NONE',  ( -7.807601069497579260, -18.53474111305376937, -1.500000000000002220 ) ) ;
#14016=CARTESIAN_POINT ( 'NONE',  ( -9.607008362728935325, -21.85066016484769236, -1.443836447538997536 ) ) ;
#14017=ORIENTED_EDGE ( 'NONE', *, *, #51529, .F. ) ;
#14019=CARTESIAN_POINT ( 'NONE',  ( 10.24050353823403192, -19.87907451059620456, -1.500000000000002220 ) ) ;
#14020=EDGE_LOOP ( 'NONE', ( #58663, #75626, #7240, #73800 ) ) ;
#14023=DIRECTION ( 'NONE',  ( -1.000000000000000000, -3.773278334444167608E-23, -8.201307833595939069E-29 ) ) ;
#14025=VECTOR ( 'NONE', #46828, 1000.000000000000114 ) ;
#14026=CARTESIAN_POINT ( 'NONE',  ( -96.62287095715012697, -23.96177878511309345, 10.65340807706330217 ) ) ;
#14027=CARTESIAN_POINT ( 'NONE',  ( 19.09806219120973125, -4.162641619376711510, 11.49999999999998934 ) ) ;
#14028=EDGE_CURVE ( 'NONE', #89948, #30324, #81958, .T. ) ;
#14029=CARTESIAN_POINT ( 'NONE',  ( -119.6228709571500559, -29.50250786944525672, 11.44777988621622811 ) ) ;
#14030=CARTESIAN_POINT ( 'NONE',  ( -8.943896628894790979, 19.53434260886740503, -1.500000000000002220 ) ) ;
#14034=CARTESIAN_POINT ( 'NONE',  ( -120.5228709571500616, -24.83602698348161653, 1.605859176311263736 ) ) ;
#14036=CARTESIAN_POINT ( 'NONE',  ( -7.756741253720922380, -21.46081514045699024, -1.500000000000002220 ) ) ;
#14038=CARTESIAN_POINT ( 'NONE',  ( -106.5596227115201344, -23.48786465467241769, 11.44779295918253403 ) ) ;
#14039=LINE ( 'NONE', #67356, #39299 ) ;
#14040=CARTESIAN_POINT ( 'NONE',  ( 19.63333621495807435, 3.783328549194958867, 11.49999999999999645 ) ) ;
#14041=DIRECTION ( 'NONE',  ( 0.000000000000000000, -2.173523156925979552E-06, 0.9999999999976378895 ) ) ;
#14042=FACE_OUTER_BOUND ( 'NONE', #28116, .T. ) ;
#14044=VERTEX_POINT ( 'NONE', #22911 ) ;
#14046=DIRECTION ( 'NONE',  ( 3.773278334444167608E-23, -1.000000000000000000, 0.000000000000000000 ) ) ;
#14048=B_SPLINE_CURVE_WITH_KNOTS ( 'NONE', 3,
 ( #4881, #10991, #19092, #73399, #12485, #3894 ),
 .UNSPECIFIED., .F., .F.,
 ( 4, 2, 4 ),
 ( 0.000000000000000000, 0.001380764517853253371, 0.002761529035706506742 ),
 .UNSPECIFIED. ) ;
#14049=CARTESIAN_POINT ( 'NONE',  ( 20.36105213711617878, 7.643125777291208678, -1.500000000000002220 ) ) ;
#14050=CARTESIAN_POINT ( 'NONE',  ( -88.88918693012689687, -25.22391110550272941, 6.409327647371936720 ) ) ;
#14051=CARTESIAN_POINT ( 'NONE',  ( 19.03533760385612439, 4.641190475545474037, -1.500000000000002220 ) ) ;
#14053=CARTESIAN_POINT ( 'NONE',  ( -61.62287095715004881, -24.64898659630528854, 1.056161002820822592 ) ) ;
#14054=B_SPLINE_CURVE_WITH_KNOTS ( 'NONE', 3,
 ( #68470, #84180, #38013, #22766, #23270, #53753 ),
 .UNSPECIFIED., .F., .F.,
 ( 4, 2, 4 ),
 ( 1.570887131794176733E-05, 0.001396322306279757170, 0.002776935741241572803 ),
 .UNSPECIFIED. ) ;
#14057=DIRECTION ( 'NONE',  ( -3.773278334453079618E-23, 0.9999999999976377785, 2.173523156925979975E-06 ) ) ;
#14058=CARTESIAN_POINT ( 'NONE',  ( -124.5228709571500616, -23.47596703998600631, 11.44779298504227860 ) ) ;
#14059=CARTESIAN_POINT ( 'NONE',  ( 4.362881659454829197, 20.01674633476859810, 11.49999999999999645 ) ) ;
#14062=CARTESIAN_POINT ( 'NONE',  ( -49.52287095715004739, -24.66019654487198665, 8.947790411086131712 ) ) ;
#14065=CARTESIAN_POINT ( 'NONE',  ( -109.6228709571500559, -29.50250243563736774, 8.947779886222136270 ) ) ;
#14067=CARTESIAN_POINT ( 'NONE',  ( -101.6228709571500559, -23.48783264082479505, -1.443836473390062380 ) ) ;
#14069=DIRECTION ( 'NONE',  ( 0.000000000000000000, -0.9999999999976377785, -2.173523156925979975E-06 ) ) ;
#14072=AXIS2_PLACEMENT_3D ( 'NONE', #82293, #59970, #12770 ) ;
#14074=CARTESIAN_POINT ( 'NONE',  ( -10.32085834726444595, 20.65377284989807194, 11.49999999999999645 ) ) ;
#14075=CARTESIAN_POINT ( 'NONE',  ( -12.29745307268338195, -19.16510367807413218, 11.49999999999998934 ) ) ;
#14076=CARTESIAN_POINT ( 'NONE',  ( -110.5923908730569707, -24.15602025860899360, 10.28564288303534724 ) ) ;
#14077=CARTESIAN_POINT ( 'NONE',  ( -88.52287095715009002, -23.48783264082477018, -1.443836473390089692 ) ) ;
#14078=CARTESIAN_POINT ( 'NONE',  ( -77.52287095715006160, -29.50248528299804818, 1.056150453629038477 ) ) ;
#14080=CARTESIAN_POINT ( 'NONE',  ( -110.6263928191107482, -24.63355581998384380, 0.9682620441943931011 ) ) ;
#14081=CARTESIAN_POINT ( 'NONE',  ( -5.132426408838210108, -21.30661980433056968, -1.500000000000002220 ) ) ;
#14082=ADVANCED_FACE ( 'NONE', ( #85332 ), #47291, .F. ) ;
#14084=CARTESIAN_POINT ( 'NONE',  ( -50.62287095715005592, -25.00158670708909625, 2.256160236439165967 ) ) ;
#14086=CARTESIAN_POINT ( 'NONE',  ( -78.60051294073809913, -23.73766607897670511, -1.055555164236459342 ) ) ;
#14087=CARTESIAN_POINT ( 'NONE',  ( -94.62287095714998486, -24.51387760970725083, 9.387446482453411178 ) ) ;
#14088=PLANE ( 'NONE',  #66471 ) ;
#14090=B_SPLINE_CURVE_WITH_KNOTS ( 'NONE', 3,
 ( #38611, #16770, #69571, #22862 ),
 .UNSPECIFIED., .F., .F.,
 ( 4, 4 ),
 ( 0.9694772152566509815, 0.9704779622974166742 ),
 .UNSPECIFIED. ) ;
#14091=CARTESIAN_POINT ( 'NONE',  ( 11.41020680648336771, 16.95828056793917682, -1.500000000000002220 ) ) ;
#14092=EDGE_LOOP ( 'NONE', ( #56363, #65467, #74992, #60426 ) ) ;
#14093=B_SPLINE_CURVE_WITH_KNOTS ( 'NONE', 3,
 ( #81362, #5231, #83344, #90468, #59033, #11843 ),
 .UNSPECIFIED., .F., .F.,
 ( 4, 2, 4 ),
 ( 0.000000000000000000, 0.001380764517853253588, 0.002761529035706507176 ),
 .UNSPECIFIED. ) ;
#14094=ORIENTED_EDGE ( 'NONE', *, *, #90877, .F. ) ;
#14096=EDGE_LOOP ( 'NONE', ( #20714, #14226, #81878, #9383 ) ) ;
#14097=CARTESIAN_POINT ( 'NONE',  ( -21.75560140871883164, 7.562747417745157463, 11.49999999999998934 ) ) ;
#14098=CARTESIAN_POINT ( 'NONE',  ( -35.52287095715006870, -25.00158670708909270, 2.256160236439166411 ) ) ;
#14099=CARTESIAN_POINT ( 'NONE',  ( 18.19722386731275066, -8.884848157732822216, -1.500000000000002220 ) ) ;
#14102=CARTESIAN_POINT ( 'NONE',  ( -54.55620429048340014, -24.64965694238574656, 8.947790433994203596 ) ) ;
#14104=DIRECTION ( 'NONE',  ( -3.773278334453080206E-23, 0.9999999999976377785, 2.173523156925979975E-06 ) ) ;
#14105=CARTESIAN_POINT ( 'NONE',  ( -99.59917429406625899, -23.48786465467241413, 11.44779295918254292 ) ) ;
#14106=CARTESIAN_POINT ( 'NONE',  ( -20.93543047832761417, 4.563121699532205255, 11.49999999999999645 ) ) ;
#14109=CARTESIAN_POINT ( 'NONE',  ( -105.5228709571500616, -29.50249982740957577, 7.747779886224967605 ) ) ;
#14110=ORIENTED_EDGE ( 'NONE', *, *, #78539, .T. ) ;
#14112=CARTESIAN_POINT ( 'NONE',  ( -19.90621922972506397, 5.769413876575915978, -1.500000000000002220 ) ) ;
#14116=CARTESIAN_POINT ( 'NONE',  ( -28.57983198641674250, -24.35651115837791281, 0.6176551810875500204 ) ) ;
#14117=VERTEX_POINT ( 'NONE', #55409 ) ;
#14120=CARTESIAN_POINT ( 'NONE',  ( -5.787726610425443674, -20.20099407548119075, -1.500000000000002220 ) ) ;
#14121=CARTESIAN_POINT ( 'NONE',  ( -21.86317675896206225, -2.224439152981679602, 11.49999999999999645 ) ) ;
#14122=CARTESIAN_POINT ( 'NONE',  ( -73.59659219034413979, -23.96169478059713143, 10.65365249895718236 ) ) ;
#14123=CARTESIAN_POINT ( 'NONE',  ( 6.936750662203477802, 21.44973376661030429, -1.500000000000002220 ) ) ;
#14125=CARTESIAN_POINT ( 'NONE',  ( -13.85205798638896901, 15.75786377350088507, 11.49999999999998934 ) ) ;
#14127=CARTESIAN_POINT ( 'NONE',  ( -89.23534077628077910, -25.26877915520014994, 5.947789088310639904 ) ) ;
#14129=VERTEX_POINT ( 'NONE', #84837 ) ;
#14131=EDGE_LOOP ( 'NONE', ( #69347, #4997, #87419, #19593 ) ) ;
#14134=CARTESIAN_POINT ( 'NONE',  ( 21.44729954461699251, -1.519088741117538000, -1.500000000000002220 ) ) ;
#14136=VERTEX_POINT ( 'NONE', #15317 ) ;
#14137=CARTESIAN_POINT ( 'NONE',  ( 5.126256225908648823, -20.47799061884807870, 11.49999999999998934 ) ) ;
#14138=DIRECTION ( 'NONE',  ( -3.773278334453079618E-23, 0.9999999999976377785, 2.173523156925979975E-06 ) ) ;
#14139=CARTESIAN_POINT ( 'NONE',  ( -64.54880478395197940, -24.15543982623906416, -0.2315651400026674800 ) ) ;
#14140=CARTESIAN_POINT ( 'NONE',  ( -50.38822539166533687, -25.30267106383720943, 4.736250553104468075 ) ) ;
#14143=CARTESIAN_POINT ( 'NONE',  ( -100.2745382058950128, -25.11141107491615898, 2.838304805050361868 ) ) ;
#14144=CARTESIAN_POINT ( 'NONE',  ( -5.973063517705734071, 21.31661749205449041, -1.500000000000002220 ) ) ;
#14145=CARTESIAN_POINT ( 'NONE',  ( -81.59562844260206305, -23.96169478059713498, 10.65365249895718591 ) ) ;
#14146=ADVANCED_FACE ( 'NONE', ( #93442 ), #47792, .F. ) ;
#14147=ORIENTED_EDGE ( 'NONE', *, *, #55514, .T. ) ;
#14149=CARTESIAN_POINT ( 'NONE',  ( -64.62287095715005592, -23.47593901973091235, -1.443836447539007972 ) ) ;
#14151=CARTESIAN_POINT ( 'NONE',  ( -100.5576102210739009, -23.85016227208580375, -0.8807180028928297544 ) ) ;
#14152=CARTESIAN_POINT ( 'NONE',  ( -4.672984603565591755, -18.88948546680484242, -1.500000000000002220 ) ) ;
#14153=ADVANCED_FACE ( 'NONE', ( #54903 ), #7713, .T. ) ;
#14154=CARTESIAN_POINT ( 'NONE',  ( 18.99370601119529312, 9.851043883551550806, -1.500000000000002220 ) ) ;
#14155=CARTESIAN_POINT ( 'NONE',  ( -64.62287095715005592, -24.65952944569304250, 1.056160979905695685 ) ) ;
#14156=CARTESIAN_POINT ( 'NONE',  ( -90.25584321435293589, -25.31973986624387862, 5.294390042787146200 ) ) ;
#14157=EDGE_CURVE ( 'NONE', #99250, #26538, #75829, .T. ) ;
#14158=CARTESIAN_POINT ( 'NONE',  ( -123.5228709571500758, -24.50216790748205398, 0.6166512839542613866 ) ) ;
#14159=CARTESIAN_POINT ( 'NONE',  ( -36.62287095715005592, -23.48786465467240347, 11.44779295918255180 ) ) ;
#14160=CARTESIAN_POINT ( 'NONE',  ( -11.22117850230010738, 19.66027149220947123, -1.500000000000002220 ) ) ;
#14161=ORIENTED_EDGE ( 'NONE', *, *, #93430, .T. ) ;
#14163=CARTESIAN_POINT ( 'NONE',  ( -97.62287095715005592, -24.64898659630367916, 1.056161002820829697 ) ) ;
#14164=CARTESIAN_POINT ( 'NONE',  ( -14.06767371131996214, 13.90018863433869889, 11.49999999999999645 ) ) ;
#14166=ORIENTED_EDGE ( 'NONE', *, *, #8188, .T. ) ;
#14170=CARTESIAN_POINT ( 'NONE',  ( -8.642975711230413083, 19.83371042614930957, 11.49999999999998934 ) ) ;
#14172=CARTESIAN_POINT ( 'NONE',  ( -27.53165725413984788, -24.78898537453293116, 7.599094992256131498 ) ) ;
#14173=CARTESIAN_POINT ( 'NONE',  ( 1.664315604108443925, 19.36118569274438528, -1.500000000000002220 ) ) ;
#14175=DIRECTION ( 'NONE',  ( 3.773278334444166432E-23, -1.000000000000000000, 0.000000000000000000 ) ) ;
#14176=CARTESIAN_POINT ( 'NONE',  ( -12.28770250403618114, -15.54288071925545722, -1.500000000000002220 ) ) ;
#14178=B_SPLINE_CURVE_WITH_KNOTS ( 'NONE', 3,
 ( #10241, #25968, #78235, #93970, #79244, #9743, #39685, #46812 ),
 .UNSPECIFIED., .F., .F.,
 ( 4, 2, 2, 4 ),
 ( -0.001224554619866334787, -0.0002241820295893544746, 0.0007761905606876258381, 0.002776935741241578007 ),
 .UNSPECIFIED. ) ;
#14179=VECTOR ( 'NONE', #91796, 1000.000000000000114 ) ;
#14180=CARTESIAN_POINT ( 'NONE',  ( -19.77321833943668850, 4.698914572609424134, 11.49999999999999645 ) ) ;
#14181=CARTESIAN_POINT ( 'NONE',  ( -111.6228709571500417, -24.66019654487199730, 8.947790411086124607 ) ) ;
#14182=CARTESIAN_POINT ( 'NONE',  ( -46.55620429048339304, -24.66019654487198665, 8.947790411086135265 ) ) ;
#14183=B_SPLINE_CURVE_WITH_KNOTS ( 'NONE', 3,
 ( #57049, #64169, #16959, #47923, #25575, #56044 ),
 .UNSPECIFIED., .F., .F.,
 ( 4, 2, 4 ),
 ( 0.000000000000000000, 0.001380901958385389412, 0.002761803916770778824 ),
 .UNSPECIFIED. ) ;
#14184=ORIENTED_EDGE ( 'NONE', *, *, #5215, .T. ) ;
#14185=CARTESIAN_POINT ( 'NONE',  ( -30.62200344337180269, -24.13759587396042150, -0.5132947483565730717 ) ) ;
#14186=DIRECTION ( 'NONE',  ( -3.773278334453079030E-23, 0.9999999999976377785, 2.173523156925979128E-06 ) ) ;
#14190=CARTESIAN_POINT ( 'NONE',  ( -19.74138705131307248, -3.616033589355840849, 11.49999999999998934 ) ) ;
#14195=CARTESIAN_POINT ( 'NONE',  ( -21.78311099772515647, -6.823855485095160489, 11.49999999999999645 ) ) ;
#14196=CARTESIAN_POINT ( 'NONE',  ( -102.5228709571500332, -23.94994826722564696, -0.6494450866342718065 ) ) ;
#14197=CARTESIAN_POINT ( 'NONE',  ( -111.9545715455114987, -25.05712135967895193, 7.447789548357302891 ) ) ;
#14198=CARTESIAN_POINT ( 'NONE',  ( -114.6228709571500417, -24.65952944569305316, 1.056160979905703234 ) ) ;
#14205=AXIS2_PLACEMENT_3D ( 'NONE', #78549, #87684, #24769 ) ;
#14206=CARTESIAN_POINT ( 'NONE',  ( 8.194921280291850962, -18.63391395107102610, -1.500000000000002220 ) ) ;
#14207=EDGE_LOOP ( 'NONE', ( #53184, #48051, #49853, #4882 ) ) ;
#14208=B_SPLINE_CURVE_WITH_KNOTS ( 'NONE', 3,
 ( #5945, #21655, #14554, #61256 ),
 .UNSPECIFIED., .F., .F.,
 ( 4, 4 ),
 ( 0.000000000000000000, 9.999999999997510880E-05 ),
 .UNSPECIFIED. ) ;
#14209=CARTESIAN_POINT ( 'NONE',  ( 22.43992371924722917, 4.826111843257130829, -1.500000000000002220 ) ) ;
#14210=CARTESIAN_POINT ( 'NONE',  ( -95.62287095715005592, -29.50248789122583659, 2.256150453626215580 ) ) ;
#14212=CARTESIAN_POINT ( 'NONE',  ( -101.6228709571500559, -24.64965695001469115, 8.947790433994178727 ) ) ;
#14213=CARTESIAN_POINT ( 'NONE',  ( -77.60072532662823619, -23.73791477778911840, 11.05961554403170588 ) ) ;
#14214=CARTESIAN_POINT ( 'NONE',  ( -89.62287095715004170, -24.65952944569305316, 1.056160979905700348 ) ) ;
#14215=CARTESIAN_POINT ( 'NONE',  ( -21.25539211000977957, 0.9166567589900279645, 11.49999999999999645 ) ) ;
#14217=VERTEX_POINT ( 'NONE', #70621 ) ;
#14218=CARTESIAN_POINT ( 'NONE',  ( 10.53326394202159300, -19.55463526559320542, 11.49999999999998934 ) ) ;
#14219=CARTESIAN_POINT ( 'NONE',  ( -16.41017380093149214, -12.48182641202616416, 11.49999999999998934 ) ) ;
#14220=B_SPLINE_CURVE_WITH_KNOTS ( 'NONE', 3,
 ( #15605, #77497, #86625, #7998, #17110, #32338 ),
 .UNSPECIFIED., .F., .F.,
 ( 4, 2, 4 ),
 ( 0.000000000000000000, 0.001380764517854763665, 0.002761529035709527329 ),
 .UNSPECIFIED. ) ;
#14222=EDGE_LOOP ( 'NONE', ( #272, #51177, #9567, #100085 ) ) ;
#14223=VERTEX_POINT ( 'NONE', #94455 ) ;
#14224=DIRECTION ( 'NONE',  ( 3.773278334444167608E-23, -1.000000000000000000, 0.000000000000000000 ) ) ;
#14226=ORIENTED_EDGE ( 'NONE', *, *, #60816, .F. ) ;
#14227=EDGE_CURVE ( 'NONE', #17879, #16795, #66162, .T. ) ;
#14229=CARTESIAN_POINT ( 'NONE',  ( -125.2170248000532240, -25.23482019547912714, 3.690485340690513372 ) ) ;
#14230=CARTESIAN_POINT ( 'NONE',  ( -39.62287095715005592, -24.64965695001468404, 8.947790433994187609 ) ) ;
#14231=CARTESIAN_POINT ( 'NONE',  ( 17.18838054715250152, -11.71887806637979779, -1.500000000000002220 ) ) ;
#14232=CARTESIAN_POINT ( 'NONE',  ( 3.468383421097696928, -21.53508805063734854, 11.49999999999999645 ) ) ;
#14233=CARTESIAN_POINT ( 'NONE',  ( -40.41683116089613748, -25.27806139858977375, 5.082404452748810364 ) ) ;
#14236=CARTESIAN_POINT ( 'NONE',  ( 12.99221220249228281, -18.32192329980629708, 11.49999999999998934 ) ) ;
#14238=EDGE_CURVE ( 'NONE', #25844, #47437, #41692, .T. ) ;
#14242=LINE ( 'NONE', #37093, #76652 ) ;
#14243=B_SPLINE_SURFACE_WITH_KNOTS ( 'NONE', 3, 3, ( 
 ( #43127, #49255, #65487, #96406 ),
 ( #19764, #73575, #50740, #95903 ),
 ( #34514, #96906, #74076, #56369 ),
 ( #4568, #35517, #27400, #33508 ),
 ( #25392, #64492, #10171, #95408 ),
 ( #80183, #58359, #10673, #41636 ),
 ( #80680, #42143, #26894, #21758 ) ),
 .UNSPECIFIED., .F., .F., .F.,
 ( 4, 3, 4 ),
 ( 4, 4 ),
 ( 0.7945040050992248082, 0.8970133687736505657, 0.9995227324480764342 ),
 ( 0.6796667099735372863, 0.6809932137839499466 ),
 .UNSPECIFIED. ) ;
#14244=EDGE_CURVE ( 'NONE', #93778, #13213, #73516, .T. ) ;
#14245=ORIENTED_EDGE ( 'NONE', *, *, #62064, .F. ) ;
#14247=PLANE ( 'NONE',  #27973 ) ;
#14249=CARTESIAN_POINT ( 'NONE',  ( -6.767052838139933080, -20.26514109264706676, -1.500000000000002220 ) ) ;
#14250=ORIENTED_EDGE ( 'NONE', *, *, #26109, .F. ) ;
#14252=CARTESIAN_POINT ( 'NONE',  ( 8.881738082190086203, 19.07353979602852689, -1.500000000000002220 ) ) ;
#14253=CARTESIAN_POINT ( 'NONE',  ( -30.64649553399479132, -23.48778889868011177, -1.443836490256471983 ) ) ;
#14254=CARTESIAN_POINT ( 'NONE',  ( -55.58953762381673869, -23.47593901973091235, -1.443836447539007972 ) ) ;
#14255=PLANE ( 'NONE',  #30404 ) ;
#14256=CARTESIAN_POINT ( 'NONE',  ( 9.607415760296678542, -19.69187540195887465, -1.500000000000002220 ) ) ;
#14258=ORIENTED_EDGE ( 'NONE', *, *, #37, .T. ) ;
#14259=CARTESIAN_POINT ( 'NONE',  ( -122.6244483497931554, -24.35071581493544102, 9.817618358456019934 ) ) ;
#14262=CARTESIAN_POINT ( 'NONE',  ( -84.55097372852188187, -24.15620529776628445, 10.23563542870660292 ) ) ;
#14263=CARTESIAN_POINT ( 'NONE',  ( -128.5228709571501327, -24.51283580621458213, 0.6167428607047164002 ) ) ;
#14264=CARTESIAN_POINT ( 'NONE',  ( -20.39835522263757639, -24.35407914423024067, 7.291654623549836955 ) ) ;
#14265=CARTESIAN_POINT ( 'NONE',  ( -7.839647760473957838, 19.78794240023834661, 11.49999999999998934 ) ) ;
#14266=CARTESIAN_POINT ( 'NONE',  ( -55.62287095715007723, -24.83620972994591725, 8.398175272781369216 ) ) ;
#14267=CARTESIAN_POINT ( 'NONE',  ( -103.6228709571500417, -24.65952944569304606, 1.056160979905701680 ) ) ;
#14270=VECTOR ( 'NONE', #74720, 1000.000000000000114 ) ;
#14271=CARTESIAN_POINT ( 'NONE',  ( -33.61928056205821491, -23.48783264082477729, -1.443836473390078368 ) ) ;
#14272=CARTESIAN_POINT ( 'NONE',  ( -8.346146134265904237, -20.86121191590761015, -1.500000000000002220 ) ) ;
#14274=B_SPLINE_CURVE_WITH_KNOTS ( 'NONE', 3,
 ( #37300, #90577, #82953, #21549 ),
 .UNSPECIFIED., .F., .F.,
 ( 4, 4 ),
 ( 0.000000000000000000, 9.999999999998897304E-05 ),
 .UNSPECIFIED. ) ;
#14276=VERTEX_POINT ( 'NONE', #43184 ) ;
#14277=CARTESIAN_POINT ( 'NONE',  ( -72.58953762381672448, -23.48783264082478084, -1.443836473390067265 ) ) ;
#14278=CARTESIAN_POINT ( 'NONE',  ( -19.13235715846047214, 4.354950445902704637, 11.49999999999999645 ) ) ;
#14279=CARTESIAN_POINT ( 'NONE',  ( -68.62287095715005592, -24.64898659630367916, 1.056161002820824368 ) ) ;
#14284=CARTESIAN_POINT ( 'NONE',  ( -70.09875394134060400, -25.30475096868035223, 4.859099491364304413 ) ) ;
#14285=CARTESIAN_POINT ( 'NONE',  ( -84.58953762381672448, -23.47593901973091235, -1.443836447539004642 ) ) ;
#14286=CARTESIAN_POINT ( 'NONE',  ( -88.87045360978522979, -25.25787539255926717, 3.590294762828090125 ) ) ;
#14289=CARTESIAN_POINT ( 'NONE',  ( -13.01991350253972080, 14.82018230214031895, 11.49999999999998934 ) ) ;
#14290=EDGE_CURVE ( 'NONE', #53455, #65243, #17805, .T. ) ;
#14291=AXIS2_PLACEMENT_3D ( 'NONE', #56904, #64530, #33046 ) ;
#14293=DIRECTION ( 'NONE',  ( -3.773278334453079618E-23, 0.9999999999976377785, 2.173523156925978705E-06 ) ) ;
#14294=CARTESIAN_POINT ( 'NONE',  ( -73.52287095715007581, -29.50250786944525672, 11.44777988621623699 ) ) ;
#14300=CARTESIAN_POINT ( 'NONE',  ( -99.00488046896290939, -25.03144984087232316, 6.667020479340355799 ) ) ;
#14302=B_SPLINE_CURVE_WITH_KNOTS ( 'NONE', 3,
 ( #53051, #59163, #35329, #60172, #6366, #58658, #13965, #90107, #43933, #5863, #97713, #29698, #21080, #99198, #52543, #12966 ),
 .UNSPECIFIED., .F., .F.,
 ( 4, 2, 2, 2, 2, 2, 2, 4 ),
 ( 8.673617379884034509E-19, 0.0008744097536164322079, 0.001748819507232863548, 0.002186024384041078406, 0.002623229260849293479, 0.003060434137657508120, 0.003279036576061615440, 0.003497639014465723194 ),
 .UNSPECIFIED. ) ;
#14303=CARTESIAN_POINT ( 'NONE',  ( -70.06086327669997615, -25.24515049912487186, 5.348962429823249209 ) ) ;
#14304=CARTESIAN_POINT ( 'NONE',  ( -112.5228709571500616, -23.47593901973090524, -1.443836447538996426 ) ) ;
#14305=CARTESIAN_POINT ( 'NONE',  ( 16.79232260237064978, 10.84791536263152523, 11.49999999999998934 ) ) ;
#14306=CARTESIAN_POINT ( 'NONE',  ( -27.68651082257923335, -29.50248793196339747, 2.274893084117591613 ) ) ;
#14307=DIRECTION ( 'NONE',  ( -1.000000000000000000, -3.773278334444167608E-23, -8.201307816334959825E-29 ) ) ;
#14310=CARTESIAN_POINT ( 'NONE',  ( -119.6274264067609323, -23.73766607897670511, -1.055555164236450238 ) ) ;
#14311=CARTESIAN_POINT ( 'NONE',  ( -80.52209456291633671, -23.48786465467241058, 11.44779295918254824 ) ) ;
#14313=CARTESIAN_POINT ( 'NONE',  ( -81.59192521434273715, -24.15543982623907482, -0.2315651400026469686 ) ) ;
#14316=B_SPLINE_SURFACE_WITH_KNOTS ( 'NONE', 3, 3, ( 
 ( #82750, #73652, #50820, #66066 ),
 ( #51315, #97964, #57449, #88378 ),
 ( #12232, #97483, #43213, #43702 ),
 ( #74151, #81259, #88885, #50323 ),
 ( #18859, #58929, #42719, #4644 ),
 ( #36087, #28463, #4145, #49836 ),
 ( #59428, #35599, #5133, #82255 ) ),
 .UNSPECIFIED., .F., .F., .F.,
 ( 4, 3, 4 ),
 ( 4, 4 ),
 ( 0.7945040049422250616, 0.8970133707663761058, 0.9995227365905272610 ),
 ( 0.06486256430468022305, 0.06976587085265167909 ),
 .UNSPECIFIED. ) ;
#14318=DIRECTION ( 'NONE',  ( -3.773278334444166432E-23, 1.000000000000000000, 0.000000000000000000 ) ) ;
#14319=ORIENTED_EDGE ( 'NONE', *, *, #20047, .T. ) ;
#14320=CARTESIAN_POINT ( 'NONE',  ( -19.75413285895528404, 4.560271753130525241, -1.500000000000002220 ) ) ;
#14321=CARTESIAN_POINT ( 'NONE',  ( -122.5564249815854083, -23.73766607897671221, -1.055555164236450461 ) ) ;
#14322=DIRECTION ( 'NONE',  ( 3.773278334444166432E-23, -1.000000000000000000, 0.000000000000000000 ) ) ;
#14323=B_SPLINE_CURVE_WITH_KNOTS ( 'NONE', 3,
 ( #79451, #63761, #30779, #61749 ),
 .UNSPECIFIED., .F., .F.,
 ( 4, 4 ),
 ( 0.000000000000000000, 9.999999999998900014E-05 ),
 .UNSPECIFIED. ) ;
#14325=DIRECTION ( 'NONE',  ( 0.000000000000000000, 0.9999999999976377785, 2.173523156925979975E-06 ) ) ;
#14326=ORIENTED_EDGE ( 'NONE', *, *, #37403, .F. ) ;
#14327=CARTESIAN_POINT ( 'NONE',  ( -92.62287095715005592, -29.50250243563736774, 8.947779886222139822 ) ) ;
#14329=CARTESIAN_POINT ( 'NONE',  ( 8.649182803842551337, -18.14983140373652404, -1.500000000000002220 ) ) ;
#14330=CARTESIAN_POINT ( 'NONE',  ( -1.165634184549018126, -21.02984315360824752, 11.49999999999999645 ) ) ;
#14331=CARTESIAN_POINT ( 'NONE',  ( -83.52287095715006160, -29.50247984919015209, -1.443849546365053582 ) ) ;
#14332=CARTESIAN_POINT ( 'NONE',  ( -22.12685673520133989, -0.1325007643398395663, 11.49999999999998934 ) ) ;
#14333=CARTESIAN_POINT ( 'NONE',  ( 8.954683214801249846, 18.48387022957959047, -1.500000000000002220 ) ) ;
#14335=ADVANCED_FACE ( 'NONE', ( #60413 ), #98944, .T. ) ;
#14336=CARTESIAN_POINT ( 'NONE',  ( -53.62287095715006302, -24.51283580621364422, 0.6167428607019741493 ) ) ;
#14337=ORIENTED_EDGE ( 'NONE', *, *, #8058, .F. ) ;
#14338=DIRECTION ( 'NONE',  ( 0.000000000000000000, -0.9999999999976377785, -2.173523156925979975E-06 ) ) ;
#14339=ORIENTED_EDGE ( 'NONE', *, *, #10467, .T. ) ;
#14340=CARTESIAN_POINT ( 'NONE',  ( -47.52287095715006160, -23.48783264083458988, -1.443836473374825236 ) ) ;
#14341=CARTESIAN_POINT ( 'NONE',  ( -102.6228709571500559, -23.47596703998600631, 11.44779298504227683 ) ) ;
#14344=AXIS2_PLACEMENT_3D ( 'NONE', #48677, #47667, #31430 ) ;
#14345=ORIENTED_EDGE ( 'NONE', *, *, #64057, .F. ) ;
#14346=DIRECTION ( 'NONE',  ( -3.773278334444167608E-23, 1.000000000000000000, 0.000000000000000000 ) ) ;
#14348=CARTESIAN_POINT ( 'NONE',  ( -68.62364079698707542, -24.66019654487199375, 8.947790411086122830 ) ) ;
#14349=CARTESIAN_POINT ( 'NONE',  ( -20.66316395829706209, -0.6310838753663271516, -1.500000000000002220 ) ) ;
#14350=CARTESIAN_POINT ( 'NONE',  ( 10.40854797073303395, 18.91789161722374146, 11.49999999999999645 ) ) ;
#14351=ORIENTED_EDGE ( 'NONE', *, *, #56955, .F. ) ;
#14353=CARTESIAN_POINT ( 'NONE',  ( -96.58953762381671027, -24.64965694238407323, 8.947790433994649462 ) ) ;
#14354=CARTESIAN_POINT ( 'NONE',  ( 21.65046080595755740, -5.567969076317650590, 11.49999999999998934 ) ) ;
#14355=ADVANCED_FACE ( 'NONE', ( #58899 ), #44175, .T. ) ;
#14357=CARTESIAN_POINT ( 'NONE',  ( -48.55620429048339304, -23.48786465467240703, 11.44779295918255357 ) ) ;
#14358=FACE_OUTER_BOUND ( 'NONE', #28228, .T. ) ;
#14361=CARTESIAN_POINT ( 'NONE',  ( -49.48507484674644274, -24.66019654487198665, 8.947790411086131712 ) ) ;
#14362=B_SPLINE_CURVE_WITH_KNOTS ( 'NONE', 3,
 ( #89122, #42956, #19094, #4883, #36829, #73892 ),
 .UNSPECIFIED., .F., .F.,
 ( 4, 2, 4 ),
 ( 0.000000000000000000, 0.001380764517853249685, 0.002761529035706499369 ),
 .UNSPECIFIED. ) ;
#14363=ADVANCED_FACE ( 'NONE', ( #66544 ), #5103, .T. ) ;
#14364=CARTESIAN_POINT ( 'NONE',  ( -19.40664508603899563, 7.695215611089875729, -1.500000000000002220 ) ) ;
#14366=CARTESIAN_POINT ( 'NONE',  ( -86.55835945172226786, -23.73766607897671221, -1.055555164236433141 ) ) ;
#14369=CARTESIAN_POINT ( 'NONE',  ( -109.5591694646261658, -23.48786465467241769, 11.44779295918253759 ) ) ;
#14370=CARTESIAN_POINT ( 'NONE',  ( 17.90021246794804810, -11.17811638239879279, -1.500000000000002220 ) ) ;
#14371=ORIENTED_EDGE ( 'NONE', *, *, #18729, .F. ) ;
#14372=CARTESIAN_POINT ( 'NONE',  ( -101.9507253916653440, -25.24282061761981666, 6.236250683194342059 ) ) ;
#14373=CARTESIAN_POINT ( 'NONE',  ( -100.0836892525862254, -25.12215667151522425, 7.064315935744911457 ) ) ;
#14374=CARTESIAN_POINT ( 'NONE',  ( 6.392671032147439369, 20.83241601264130693, 11.49999999999998934 ) ) ;
#14375=FACE_OUTER_BOUND ( 'NONE', #55954, .T. ) ;
#14376=CARTESIAN_POINT ( 'NONE',  ( -81.58953762381673869, -24.64898659630528854, 1.056161002820825923 ) ) ;
#14378=CARTESIAN_POINT ( 'NONE',  ( 21.56942612084361599, 2.798134137018522427, -1.500000000000002220 ) ) ;
#14380=CARTESIAN_POINT ( 'NONE',  ( 21.63714550250683644, -5.416328558471028565, 11.49999999999999645 ) ) ;
#14381=VERTEX_POINT ( 'NONE', #29935 ) ;
#14382=CARTESIAN_POINT ( 'NONE',  ( -33.52287095715004739, -23.96127896942118696, -0.6493128930941889365 ) ) ;
#14383=LINE ( 'NONE', #53969, #3826 ) ;
#14386=VERTEX_POINT ( 'NONE', #82723 ) ;
#14387=ORIENTED_EDGE ( 'NONE', *, *, #4429, .F. ) ;
#14391=CARTESIAN_POINT ( 'NONE',  ( -9.361133326760958440, -19.03884994183470880, -1.500000000000002220 ) ) ;
#14393=CARTESIAN_POINT ( 'NONE',  ( -80.08103705783366877, -25.27791962444818097, 7.514832344495668615 ) ) ;
#14394=EDGE_CURVE ( 'NONE', #80787, #41257, #35566, .T. ) ;
#14397=CARTESIAN_POINT ( 'NONE',  ( -18.23339674026497903, -6.527145932826366348, -1.500000000000002220 ) ) ;
#14398=CARTESIAN_POINT ( 'NONE',  ( -45.57256808031284123, -23.48783264082476308, -1.443836473390102793 ) ) ;
#14400=CARTESIAN_POINT ( 'NONE',  ( -11.04204518803028456, 15.98388583709530941, 11.49999999999999645 ) ) ;
#14407=CARTESIAN_POINT ( 'NONE',  ( -70.58592565993524204, -25.30487017711728370, 4.870295994224087544 ) ) ;
#14408=AXIS2_PLACEMENT_3D ( 'NONE', #67811, #75388, #67302 ) ;
#14411=CARTESIAN_POINT ( 'NONE',  ( -19.57149217635686966, 1.386223266712492297, -1.500000000000002220 ) ) ;
#14412=CARTESIAN_POINT ( 'NONE',  ( -66.58953762381672448, -23.48786465467241058, 11.44779295918254647 ) ) ;
#14414=CARTESIAN_POINT ( 'NONE',  ( -17.67581969798968444, -12.36387604476075097, 11.49999999999998934 ) ) ;
#14416=CARTESIAN_POINT ( 'NONE',  ( -40.57795575760204088, -24.83618233451450052, 1.606449574219539267 ) ) ;
#14417=B_SPLINE_CURVE_WITH_KNOTS ( 'NONE', 3,
 ( #16826, #47789, #597, #32552 ),
 .UNSPECIFIED., .F., .F.,
 ( 4, 4 ),
 ( 0.000000000000000000, 0.0001000000000000028644 ),
 .UNSPECIFIED. ) ;
#14418=EDGE_CURVE ( 'NONE', #4416, #58649, #20312, .T. ) ;
#14419=CARTESIAN_POINT ( 'NONE',  ( -99.84936175820153892, -25.18439370342922601, 3.453118441789628346 ) ) ;
#14420=CARTESIAN_POINT ( 'NONE',  ( 19.24196208499951055, 12.69117723712289703, -1.500000000000002220 ) ) ;
#14424=CARTESIAN_POINT ( 'NONE',  ( 19.31759285448427477, -5.727529672960866236, 11.49999999999999645 ) ) ;
#14425=CARTESIAN_POINT ( 'NONE',  ( -71.52287095715006160, -23.47593901973090169, -1.443836447538996870 ) ) ;
#14426=DIRECTION ( 'NONE',  ( 0.000000000000000000, -0.9999999999976377785, -2.173523156925979975E-06 ) ) ;
#14428=CARTESIAN_POINT ( 'NONE',  ( -94.52287095715006160, -23.48786465467242479, 11.44779295918254292 ) ) ;
#14430=CARTESIAN_POINT ( 'NONE',  ( -122.5228709571501327, -23.96177878511310055, 10.65340807706329507 ) ) ;
#14431=CARTESIAN_POINT ( 'NONE',  ( -1.345660788846553935, -19.86331345790170033, -1.500000000000002220 ) ) ;
#14432=DIRECTION ( 'NONE',  ( 0.000000000000000000, 2.173523156925980399E-06, -0.9999999999976378895 ) ) ;
#14433=CARTESIAN_POINT ( 'NONE',  ( -10.52764212615999639, 16.74383705166681580, -1.500000000000002220 ) ) ;
#14434=CARTESIAN_POINT ( 'NONE',  ( -114.6228709571500559, -29.50247984919015209, -1.443849546365048253 ) ) ;
#14435=B_SPLINE_CURVE_WITH_KNOTS ( 'NONE', 3,
 ( #66014, #96934, #11198, #65515 ),
 .UNSPECIFIED., .F., .F.,
 ( 4, 4 ),
 ( 0.000000000000000000, 0.0001000000000000167422 ),
 .UNSPECIFIED. ) ;
#14437=CARTESIAN_POINT ( 'NONE',  ( -123.5895376238167245, -23.47596703998600631, 11.44779298504227683 ) ) ;
#14438=CARTESIAN_POINT ( 'NONE',  ( -66.52287095715007581, -23.47593901973090524, -1.443836447538997092 ) ) ;
#14439=CARTESIAN_POINT ( 'NONE',  ( 8.970943996638910178, -18.66293075132952950, 11.49999999999999645 ) ) ;
#14440=CARTESIAN_POINT ( 'NONE',  ( -58.52287095715006870, -23.94994826722565406, -0.6494450866342742490 ) ) ;
#14441=CARTESIAN_POINT ( 'NONE',  ( -49.52475239181693212, -25.25138750780670449, 5.557101021734769830 ) ) ;
#14442=AXIS2_PLACEMENT_3D ( 'NONE', #76436, #84062, #59241 ) ;
#14443=CARTESIAN_POINT ( 'NONE',  ( 10.71911242904675987, 20.06137936439360203, 11.49999999999999645 ) ) ;
#14445=CARTESIAN_POINT ( 'NONE',  ( -60.62287095715004881, -24.63287334234180292, 0.9662140553045425184 ) ) ;
#14446=CARTESIAN_POINT ( 'NONE',  ( -52.52287095715006870, -23.47596703998600631, 11.44779298504229104 ) ) ;
#14447=CARTESIAN_POINT ( 'NONE',  ( 16.36621611169882229, 11.82581248522330064, 11.49999999999998934 ) ) ;
#14449=CARTESIAN_POINT ( 'NONE',  ( -95.62287095715007013, -24.62226745350436730, 0.9660975649728198444 ) ) ;
#14450=ORIENTED_EDGE ( 'NONE', *, *, #2074, .T. ) ;
#14451=B_SPLINE_CURVE_WITH_KNOTS ( 'NONE', 3,
 ( #50029, #97680, #56644, #33789 ),
 .UNSPECIFIED., .F., .F.,
 ( 4, 4 ),
 ( 0.000000000000000000, 0.0001000000000000167422 ),
 .UNSPECIFIED. ) ;
#14454=CARTESIAN_POINT ( 'NONE',  ( -12.24191887126339751, 19.33842681661653984, 11.49999999999998934 ) ) ;
#14455=CARTESIAN_POINT ( 'NONE',  ( -41.68231076359069220, -25.22297927556520492, 3.502281763462448350 ) ) ;
#14456=CARTESIAN_POINT ( 'NONE',  ( 3.837509532605410278, -21.31939230324424628, -1.500000000000002220 ) ) ;
#14459=CARTESIAN_POINT ( 'NONE',  ( -12.66259425867894350, -16.64798919286708667, 11.49999999999999645 ) ) ;
#14461=FACE_OUTER_BOUND ( 'NONE', #62843, .T. ) ;
#14462=CARTESIAN_POINT ( 'NONE',  ( -9.458160343781703006, 19.84743614482962926, 11.49999999999998934 ) ) ;
#14463=CARTESIAN_POINT ( 'NONE',  ( -105.5573383875179303, -23.85049219812686871, 10.88485053497526955 ) ) ;
#14464=CARTESIAN_POINT ( 'NONE',  ( -28.74184145762639631, -25.21724881489072345, 7.085837703947976074 ) ) ;
#14467=CARTESIAN_POINT ( 'NONE',  ( -90.59124612480250960, -24.40133493613050675, 9.663955038902805939 ) ) ;
#14468=VERTEX_POINT ( 'NONE', #21313 ) ;
#14469=CARTESIAN_POINT ( 'NONE',  ( -72.49563018961239891, -24.66019654487199730, 8.947790411086121054 ) ) ;
#14471=VERTEX_POINT ( 'NONE', #37554 ) ;
#14474=EDGE_CURVE ( 'NONE', #84745, #73391, #22623, .T. ) ;
#14475=B_SPLINE_CURVE_WITH_KNOTS ( 'NONE', 3,
 ( #18376, #42733, #27989, #66583 ),
 .UNSPECIFIED., .F., .F.,
 ( 4, 4 ),
 ( 0.000000000000000000, 0.0004038461538461851630 ),
 .UNSPECIFIED. ) ;
#14477=CARTESIAN_POINT ( 'NONE',  ( -59.58953762381672448, -23.47593901973091235, -1.443836447539007972 ) ) ;
#14479=CARTESIAN_POINT ( 'NONE',  ( -57.61196719931660937, -23.48783264082477018, -1.443836473390095243 ) ) ;
#14480=CARTESIAN_POINT ( 'NONE',  ( -8.751980504941329286, -18.49744413911281882, -1.500000000000002220 ) ) ;
#14481=EDGE_CURVE ( 'NONE', #46348, #10120, #44406, .T. ) ;
#14482=ORIENTED_EDGE ( 'NONE', *, *, #50639, .T. ) ;
#14483=CARTESIAN_POINT ( 'NONE',  ( -93.55620429048337883, -24.64965694238574656, 8.947790433994196491 ) ) ;
#14486=EDGE_CURVE ( 'NONE', #34072, #9990, #80700, .T. ) ;
#14489=VERTEX_POINT ( 'NONE', #32442 ) ;
#14492=CARTESIAN_POINT ( 'NONE',  ( -64.55620429048339304, -23.48786465467241058, 11.44779295918254824 ) ) ;
#14494=CARTESIAN_POINT ( 'NONE',  ( 20.75994597877129877, -1.272245555857973054, 11.49999999999998934 ) ) ;
#14496=CARTESIAN_POINT ( 'NONE',  ( -101.5228709571500758, -29.50250786944525672, 11.44777988621623166 ) ) ;
#14499=CARTESIAN_POINT ( 'NONE',  ( -50.40445135320379677, -25.12217862631780108, 7.101635560799164359 ) ) ;
#14501=ORIENTED_EDGE ( 'NONE', *, *, #85401, .T. ) ;
#14503=CARTESIAN_POINT ( 'NONE',  ( -107.5228709571500758, -29.50250243563736774, 8.947779886222136270 ) ) ;
#14505=CARTESIAN_POINT ( 'NONE',  ( -119.4728709570018879, -25.30556169000782418, 4.803960565675224892 ) ) ;
#14506=CARTESIAN_POINT ( 'NONE',  ( -100.5925999562403490, -25.03152448450452638, 7.559861489817380154 ) ) ;
#14507=CARTESIAN_POINT ( 'NONE',  ( -92.50480874862623182, -24.66019654487200441, 8.947790411086117501 ) ) ;
#14508=CARTESIAN_POINT ( 'NONE',  ( -73.58953762381673869, -24.66019654487199020, 8.947790411086135265 ) ) ;
#14509=CARTESIAN_POINT ( 'NONE',  ( 12.08182546098005972, -18.57710416600862402, 11.49999999999999645 ) ) ;
#14510=ORIENTED_EDGE ( 'NONE', *, *, #89344, .F. ) ;
#14512=CARTESIAN_POINT ( 'NONE',  ( -11.22117850230010738, 19.66027149220947123, 11.49999999999998934 ) ) ;
#14513=CARTESIAN_POINT ( 'NONE',  ( -115.6323228635793896, -23.48786465467241769, 11.44779295918253581 ) ) ;
#14514=ORIENTED_EDGE ( 'NONE', *, *, #25631, .F. ) ;
#14515=VERTEX_POINT ( 'NONE', #77600 ) ;
#14516=CARTESIAN_POINT ( 'NONE',  ( -99.55620429048339304, -24.65952944569304961, 1.056160979905704345 ) ) ;
#14517=B_SPLINE_CURVE_WITH_KNOTS ( 'NONE', 3,
 ( #20859, #66582, #21351, #51832, #97494, #52327 ),
 .UNSPECIFIED., .F., .F.,
 ( 4, 2, 4 ),
 ( 0.000000000000000000, 0.001380901958385383774, 0.002761803916770767548 ),
 .UNSPECIFIED. ) ;
#14518=B_SPLINE_CURVE_WITH_KNOTS ( 'NONE', 3,
 ( #77300, #16916, #76794, #94037, #71213, #62107 ),
 .UNSPECIFIED., .F., .F.,
 ( 4, 2, 4 ),
 ( 0.000000000000000000, 0.001380901958385387894, 0.002761803916770775788 ),
 .UNSPECIFIED. ) ;
#14519=CARTESIAN_POINT ( 'NONE',  ( -20.09103079077430820, 1.113595961413322177, 11.49999999999998934 ) ) ;
#14520=B_SPLINE_SURFACE_WITH_KNOTS ( 'NONE', 3, 1, ( 
 ( #24685, #70886 ),
 ( #10977, #55668 ),
 ( #57173, #48045 ),
 ( #32309, #25190 ),
 ( #16573, #93700 ),
 ( #56167, #17586 ),
 ( #48558, #88109 ),
 ( #62786, #49552 ),
 ( #33812, #79485 ),
 ( #78975, #95713 ),
 ( #63283, #55168 ),
 ( #40926, #24191 ),
 ( #79981, #41942 ),
 ( #72884, #47548 ),
 ( #94200, #39923 ),
 ( #17081, #9472 ),
 ( #2372, #40432 ),
 ( #33303, #95214 ),
 ( #56670, #18087 ) ),
 .UNSPECIFIED., .F., .F., .F.,
 ( 4, 1, 1, 1, 1, 1, 1, 1, 1, 1, 1, 1, 1, 1, 1, 1, 4 ),
 ( 2, 2 ),
 ( 0.000000000000000000, 0.06535138202659385165, 0.1279160318306120925, 0.1883602055716991353, 0.2472160772654510563, 0.3056301291974100054, 0.3637698398318218729, 0.4226609139127802117, 0.4826872940903894071, 0.5433002212395561248, 0.6041179553231045274, 0.6649648912652841304, 0.7274134941125618425, 0.7914676251494242587, 0.8580554427290951747, 0.9270368146149470245, 1.000000000000000000 ),
 ( 0.000000000000000000, 1.000000000000000000 ),
 .UNSPECIFIED. ) ;
#14523=CARTESIAN_POINT ( 'NONE',  ( -126.5228709571501753, -23.96127896941633750, -0.6493128931037959184 ) ) ;
#14524=CARTESIAN_POINT ( 'NONE',  ( 17.53502452033532677, 13.85421504792973479, -1.500000000000002220 ) ) ;
#14527=CARTESIAN_POINT ( 'NONE',  ( -34.62287095715005592, -23.47593901973091235, -1.443836447539013301 ) ) ;
#14529=DIRECTION ( 'NONE',  ( -3.773278334453080206E-23, 0.9999999999976377785, 2.173523156925979975E-06 ) ) ;
#14531=CARTESIAN_POINT ( 'NONE',  ( -47.62287095715004881, -24.64898659630367916, 1.056161002820821038 ) ) ;
#14532=PLANE ( 'NONE',  #25338 ) ;
#14533=CARTESIAN_POINT ( 'NONE',  ( -4.042178566331402045, 19.10766070095605684, -1.500000000000002220 ) ) ;
#14534=CARTESIAN_POINT ( 'NONE',  ( -43.52287095715006160, -29.50250786944525672, 11.44777988621624232 ) ) ;
#14535=CARTESIAN_POINT ( 'NONE',  ( 7.480126432006339421, -20.11416664461015458, 11.49999999999998934 ) ) ;
#14537=DIRECTION ( 'NONE',  ( -3.773278334453079618E-23, 0.9999999999976377785, 2.173523156925978705E-06 ) ) ;
#14538=DIRECTION ( 'NONE',  ( -3.773278334453080206E-23, 0.9999999999976377785, 2.173523156925979975E-06 ) ) ;
#14541=CARTESIAN_POINT ( 'NONE',  ( -2.380104427745746154, 22.76713797270899065, -1.500000000000002220 ) ) ;
#14546=CARTESIAN_POINT ( 'NONE',  ( -14.92271332039470444, 13.28099397388983327, 11.49999999999999645 ) ) ;
#14549=CARTESIAN_POINT ( 'NONE',  ( -123.6228709571500559, -23.47593901973091235, -1.443836447538997536 ) ) ;
#14551=B_SPLINE_CURVE_WITH_KNOTS ( 'NONE', 3,
 ( #19288, #66004, #44138, #43639, #21278, #74577 ),
 .UNSPECIFIED., .F., .F.,
 ( 4, 2, 4 ),
 ( 6.384118678619858489E-06, 0.001386860460828383441, 0.002767336802978146663 ),
 .UNSPECIFIED. ) ;
#14553=FACE_OUTER_BOUND ( 'NONE', #65727, .T. ) ;
#14554=CARTESIAN_POINT ( 'NONE',  ( -70.55620429048339304, -23.48786465467240703, 11.44779295918254647 ) ) ;
#14555=CARTESIAN_POINT ( 'NONE',  ( -8.443908442993951269, 20.02826104456839218, 11.49999999999998934 ) ) ;
#14557=B_SPLINE_CURVE_WITH_KNOTS ( 'NONE', 3,
 ( #87598, #40919, #96697, #27199, #95704, #58154 ),
 .UNSPECIFIED., .F., .F.,
 ( 4, 2, 4 ),
 ( 6.384118678609746610E-06, 0.001386860460828372816, 0.002767336802978135821 ),
 .UNSPECIFIED. ) ;
#14559=CARTESIAN_POINT ( 'NONE',  ( -15.96901387740391343, -11.39031854172415947, -1.500000000000002220 ) ) ;
#14560=CARTESIAN_POINT ( 'NONE',  ( -55.52287095715005449, -29.50249982740957577, 7.747779886224967605 ) ) ;
#14566=CARTESIAN_POINT ( 'NONE',  ( -19.23287947355762384, -7.152392467615741545, 11.49999999999999645 ) ) ;
#14568=CARTESIAN_POINT ( 'NONE',  ( -53.62287095715005592, -23.47596703998600276, 11.44779298504227683 ) ) ;
#14569=AXIS2_PLACEMENT_3D ( 'NONE', #24510, #16903, #55989 ) ;
#14572=CARTESIAN_POINT ( 'NONE',  ( -51.55620429048340014, -23.47593901973091235, -1.443836447539009749 ) ) ;
#14574=CARTESIAN_POINT ( 'NONE',  ( -44.62287095715004881, -29.50247984919015209, -1.443849546365060466 ) ) ;
#14576=CARTESIAN_POINT ( 'NONE',  ( -124.6228709571500701, -24.66019654487200086, 8.947790411086121054 ) ) ;
#14578=CARTESIAN_POINT ( 'NONE',  ( 1.702247502073919394, 23.03039350466679025, 11.49999999999999645 ) ) ;
#14579=CARTESIAN_POINT ( 'NONE',  ( -2.657479817400386413, -22.66247145590962120, 11.49999999999998934 ) ) ;
#14580=DIRECTION ( 'NONE',  ( -3.773278334453079618E-23, 0.9999999999976377785, 2.173523156925979975E-06 ) ) ;
#14581=CARTESIAN_POINT ( 'NONE',  ( -105.6228709571500417, -24.99132157543166954, 2.256160258750667502 ) ) ;
#14582=CARTESIAN_POINT ( 'NONE',  ( -123.5228709571501042, -23.96127896941632685, -0.6493128931037979168 ) ) ;
#14583=DIRECTION ( 'NONE',  ( -1.000000000000000000, -3.773278334444167608E-23, -8.201307833595939069E-29 ) ) ;
#14584=CARTESIAN_POINT ( 'NONE',  ( -110.6256086358791748, -24.73486907724917572, 1.287355809206965240 ) ) ;
#14585=CARTESIAN_POINT ( 'NONE',  ( 16.40513048700843513, 14.50174154637248591, -1.500000000000002220 ) ) ;
#14586=CARTESIAN_POINT ( 'NONE',  ( -54.52287095715005449, -23.48783264082476308, -1.443836473390096797 ) ) ;
#14587=CARTESIAN_POINT ( 'NONE',  ( -50.62287095715004170, -23.48783264082478084, -1.443836473390070596 ) ) ;
#14588=DIRECTION ( 'NONE',  ( -0.000000000000000000, 2.173523156925979552E-06, -0.9999999999976378895 ) ) ;
#14590=PLANE ( 'NONE',  #17702 ) ;
#14591=LINE ( 'NONE', #5987, #33992 ) ;
#14592=ORIENTED_EDGE ( 'NONE', *, *, #79352, .F. ) ;
#14595=CARTESIAN_POINT ( 'NONE',  ( 10.07161678670223637, 17.78519941539584792, 11.49999999999998934 ) ) ;
#14599=EDGE_LOOP ( 'NONE', ( #92966, #3016, #23895, #61299 ) ) ;
#14600=CARTESIAN_POINT ( 'NONE',  ( -20.21456430084473155, -11.12997698910670152, -1.500000000000002220 ) ) ;
#14601=CARTESIAN_POINT ( 'NONE',  ( -61.55970283376174734, -23.73766607897670156, -1.055555164236459342 ) ) ;
#14602=CARTESIAN_POINT ( 'NONE',  ( 19.68333694646799614, 4.735253856516091098, -1.500000000000002220 ) ) ;
#14603=ADVANCED_FACE ( 'NONE', ( #30937 ), #27248, .T. ) ;
#14604=ORIENTED_EDGE ( 'NONE', *, *, #3918, .T. ) ;
#14605=CARTESIAN_POINT ( 'NONE',  ( -122.5228709571501042, -23.72747288104470442, -1.053458166803224794 ) ) ;
#14606=LINE ( 'NONE', #36951, #78959 ) ;
#14608=CARTESIAN_POINT ( 'NONE',  ( -28.52287095715005805, -24.48903441264110015, 8.947790432046794251 ) ) ;
#14609=CARTESIAN_POINT ( 'NONE',  ( -70.59202623176527425, -24.40034930558990922, 0.3402023900116040167 ) ) ;
#14610=CARTESIAN_POINT ( 'NONE',  ( 10.45947017991876926, -18.73710855793504848, 11.49999999999999645 ) ) ;
#14612=PLANE ( 'NONE',  #58190 ) ;
#14614=ADVANCED_FACE ( 'NONE', ( #10103 ), #57791, .T. ) ;
#14615=ORIENTED_EDGE ( 'NONE', *, *, #64753, .F. ) ;
#14617=B_SPLINE_CURVE_WITH_KNOTS ( 'NONE', 3,
 ( #95942, #86824, #79712, #65526 ),
 .UNSPECIFIED., .F., .F.,
 ( 4, 4 ),
 ( 5.880066517545130343E-09, 0.0003976749849169158076 ),
 .UNSPECIFIED. ) ;
#14618=CARTESIAN_POINT ( 'NONE',  ( -19.40401905104624802, 7.283777608679691262, 11.49999999999998934 ) ) ;
#14619=AXIS2_PLACEMENT_3D ( 'NONE', #66307, #98213, #67800 ) ;
#14622=CARTESIAN_POINT ( 'NONE',  ( -91.52287095715009002, -23.73934037231757443, 11.05740245334328442 ) ) ;
#14623=ORIENTED_EDGE ( 'NONE', *, *, #26180, .T. ) ;
#14627=CARTESIAN_POINT ( 'NONE',  ( -17.28599015371049674, 13.57978550619682956, 11.49999999999999645 ) ) ;
#14629=CARTESIAN_POINT ( 'NONE',  ( 9.831018646898828095, -20.30805102056165623, 11.49999999999998934 ) ) ;
#14630=CARTESIAN_POINT ( 'NONE',  ( -8.674659061502078217, -19.08593140856894621, -1.500000000000002220 ) ) ;
#14633=ORIENTED_EDGE ( 'NONE', *, *, #63259, .F. ) ;
#14635=ORIENTED_EDGE ( 'NONE', *, *, #97220, .T. ) ;
#14636=VECTOR ( 'NONE', #67157, 1000.000000000000114 ) ;
#14637=B_SPLINE_CURVE_WITH_KNOTS ( 'NONE', 3,
 ( #55014, #46391, #53021, #77322 ),
 .UNSPECIFIED., .F., .F.,
 ( 4, 4 ),
 ( 0.000000000000000000, 9.999999999998897304E-05 ),
 .UNSPECIFIED. ) ;
#14638=ORIENTED_EDGE ( 'NONE', *, *, #53289, .T. ) ;
#14639=CARTESIAN_POINT ( 'NONE',  ( -78.62287095715005592, -29.50248528299804818, 1.056150453629038477 ) ) ;
#14641=CARTESIAN_POINT ( 'NONE',  ( -14.25192491085926072, -16.12266454619898326, -1.500000000000002220 ) ) ;
#14642=CARTESIAN_POINT ( 'NONE',  ( -90.62287095715004170, -23.47596703998600631, 11.44779298504227860 ) ) ;
#14643=ORIENTED_EDGE ( 'NONE', *, *, #7604, .T. ) ;
#14644=CARTESIAN_POINT ( 'NONE',  ( -21.11812214938331422, 0.5215410354952813021, 11.49999999999998934 ) ) ;
#14645=CARTESIAN_POINT ( 'NONE',  ( -31.52287095715006160, -29.50250243563736774, 8.947779886222150481 ) ) ;
#14646=DIRECTION ( 'NONE',  ( -3.773278334453079030E-23, 0.9999999999976377785, 2.173523156925979128E-06 ) ) ;
#14648=PLANE ( 'NONE',  #21582 ) ;
#14650=CARTESIAN_POINT ( 'NONE',  ( 9.120982285578694615, 20.23247719416018242, -1.500000000000002220 ) ) ;
#14651=CARTESIAN_POINT ( 'NONE',  ( -81.55862828805493336, -23.73791477778911840, 11.05961554403170943 ) ) ;
#14652=EDGE_CURVE ( 'NONE', #70610, #71832, #28561, .T. ) ;
#14653=ORIENTED_EDGE ( 'NONE', *, *, #79561, .F. ) ;
#14654=CARTESIAN_POINT ( 'NONE',  ( -51.66594184980125704, -25.24860094318730219, 5.409172948272988002 ) ) ;
#14655=DIRECTION ( 'NONE',  ( -3.773278334453079618E-23, 0.9999999999976377785, 2.173523156925979975E-06 ) ) ;
#14658=CARTESIAN_POINT ( 'NONE',  ( -119.6228709571500559, -24.64898659630368627, 1.056161002820833028 ) ) ;
#14659=B_SPLINE_CURVE_WITH_KNOTS ( 'NONE', 3,
 ( #60735, #50252, #11669, #50750 ),
 .UNSPECIFIED., .F., .F.,
 ( 4, 4 ),
 ( 0.000000000000000000, 9.999999999998897304E-05 ),
 .UNSPECIFIED. ) ;
#14660=CARTESIAN_POINT ( 'NONE',  ( -8.858824863812619910, -17.32749669425128047, -1.500000000000002220 ) ) ;
#14661=CARTESIAN_POINT ( 'NONE',  ( -18.60337119584764665, 10.53494341765418874, 11.49999999999998934 ) ) ;
#14662=FACE_OUTER_BOUND ( 'NONE', #47596, .T. ) ;
#14664=CARTESIAN_POINT ( 'NONE',  ( -122.5562042904833930, -24.64965694238575367, 8.947790433994191162 ) ) ;
#14666=CARTESIAN_POINT ( 'NONE',  ( -0.4833002549469566644, -22.66139224067150337, -1.500000000000002220 ) ) ;
#14667=ORIENTED_EDGE ( 'NONE', *, *, #75188, .T. ) ;
#14668=EDGE_CURVE ( 'NONE', #56734, #22424, #65424, .T. ) ;
#14669=CARTESIAN_POINT ( 'NONE',  ( -110.5228709571500616, -25.00182538069145366, 7.747789668545101094 ) ) ;
#14670=CARTESIAN_POINT ( 'NONE',  ( -62.62287095715003460, -24.51387760970724372, 9.387446482453428942 ) ) ;
#14671=CARTESIAN_POINT ( 'NONE',  ( -18.24533751216517885, 7.751685665592884078, 11.49999999999999645 ) ) ;
#14674=EDGE_CURVE ( 'NONE', #49194, #66916, #87878, .T. ) ;
#14676=CARTESIAN_POINT ( 'NONE',  ( -57.52287095715003318, -23.48783264082476663, -1.443836473390093911 ) ) ;
#14677=CARTESIAN_POINT ( 'NONE',  ( 19.51036611237648088, 9.378288983258578071, 11.49999999999998934 ) ) ;
#14678=CARTESIAN_POINT ( 'NONE',  ( -49.14425558977711006, -25.10935316468142986, 3.703948968546024290 ) ) ;
#14679=CARTESIAN_POINT ( 'NONE',  ( -16.21482014894483470, 10.69450053600103345, -1.500000000000002220 ) ) ;
#14681=CARTESIAN_POINT ( 'NONE',  ( -82.62287095715005592, -24.51387760970725793, 9.387446482453437824 ) ) ;
#14682=CARTESIAN_POINT ( 'NONE',  ( -14.51517298184297289, -13.48802281452852725, -1.500000000000002220 ) ) ;
#14684=CARTESIAN_POINT ( 'NONE',  ( -20.07547297788957152, 3.163885811906596679, 11.49999999999999645 ) ) ;
#14685=CARTESIAN_POINT ( 'NONE',  ( -106.6228709571500559, -24.64898659630368627, 1.056161002820831474 ) ) ;
#14689=EDGE_LOOP ( 'NONE', ( #52649, #99041, #30132, #25753 ) ) ;
#14690=CARTESIAN_POINT ( 'NONE',  ( -30.63234162661936111, -23.86952536761623023, -1.017619990082605508 ) ) ;
#14692=CARTESIAN_POINT ( 'NONE',  ( -49.74369414166532977, -25.31601817158193057, 4.940877927940857894 ) ) ;
#14693=CARTESIAN_POINT ( 'NONE',  ( -40.58501377093656970, -24.63419186844611630, 9.035850630976923981 ) ) ;
#14694=CARTESIAN_POINT ( 'NONE',  ( -32.99388727629348494, -25.11010231571544082, 2.831122766524410750 ) ) ;
#14695=CARTESIAN_POINT ( 'NONE',  ( -19.91332876899582160, 2.521106391696132931, -1.500000000000002220 ) ) ;
#14696=FACE_OUTER_BOUND ( 'NONE', #99076, .T. ) ;
#14699=VECTOR ( 'NONE', #22383, 1000.000000000000114 ) ;
#14700=CARTESIAN_POINT ( 'NONE',  ( 19.54225192528841859, -11.95493969655435151, 11.49999999999999645 ) ) ;
#14701=CARTESIAN_POINT ( 'NONE',  ( 15.30562342774392093, -16.77826389816909725, 11.49999999999998934 ) ) ;
#14702=CARTESIAN_POINT ( 'NONE',  ( -49.76261995625480949, -25.31297168719047619, 4.511523210314938304 ) ) ;
#14704=CARTESIAN_POINT ( 'NONE',  ( -38.48002663928881617, -24.66019654487199375, 8.947790411086119278 ) ) ;
#14705=AXIS2_PLACEMENT_3D ( 'NONE', #37082, #83252, #13733 ) ;
#14706=CARTESIAN_POINT ( 'NONE',  ( -71.58953762381672448, -24.64898659630528854, 1.056161002820822370 ) ) ;
#14708=CARTESIAN_POINT ( 'NONE',  ( -34.52287095715006160, -24.65952944569303895, 1.056160979905690134 ) ) ;
#14709=ORIENTED_EDGE ( 'NONE', *, *, #20096, .T. ) ;
#14710=CARTESIAN_POINT ( 'NONE',  ( -14.79517943714664518, -13.99575967537150412, -1.500000000000002220 ) ) ;
#14711=ORIENTED_EDGE ( 'NONE', *, *, #16471, .F. ) ;
#14712=ADVANCED_FACE ( 'NONE', ( #41061 ), #18296, .T. ) ;
#14713=CARTESIAN_POINT ( 'NONE',  ( 7.334040449947802465, -21.76207178258647090, -1.500000000000002220 ) ) ;
#14714=CARTESIAN_POINT ( 'NONE',  ( -119.5228709571500758, -24.65952944569305316, 1.056160979905705899 ) ) ;
#14715=ORIENTED_EDGE ( 'NONE', *, *, #77253, .F. ) ;
#14716=CARTESIAN_POINT ( 'NONE',  ( -38.62287095715005592, -24.33832256526968507, 0.1851278514119830965 ) ) ;
#14717=CARTESIAN_POINT ( 'NONE',  ( -116.5228709571500332, -24.66019654487200086, 8.947790411086113949 ) ) ;
#14718=CARTESIAN_POINT ( 'NONE',  ( -51.48599270264783456, -24.66019654487199730, 8.947790411086117501 ) ) ;
#14719=CARTESIAN_POINT ( 'NONE',  ( 20.49604761983493972, 5.601127818285958071, 11.49999999999999645 ) ) ;
#14722=VERTEX_POINT ( 'NONE', #37439 ) ;
#14723=CARTESIAN_POINT ( 'NONE',  ( 21.93305185196877360, -3.456643806985262302, 11.49999999999998934 ) ) ;
#14724=ADVANCED_FACE ( 'NONE', ( #13584 ), #81617, .T. ) ;
#14725=CARTESIAN_POINT ( 'NONE',  ( -7.709890279958820258, -19.11728055126480186, 11.49999999999998934 ) ) ;
#14726=EDGE_LOOP ( 'NONE', ( #15138, #22998, #81646, #48844 ) ) ;
#14728=CARTESIAN_POINT ( 'NONE',  ( -109.7388188129343831, -25.27682897105086823, 5.649347691802135252 ) ) ;
#14729=CARTESIAN_POINT ( 'NONE',  ( -36.58953762381673158, -24.64898659630367916, 1.056161002820378725 ) ) ;
#14731=CARTESIAN_POINT ( 'NONE',  ( -91.58852912192975282, -24.34968618360934656, 0.1864209137778843617 ) ) ;
#14734=CARTESIAN_POINT ( 'NONE',  ( -88.58953762381669605, -24.66019654487199375, 8.947790411086117501 ) ) ;
#14735=CARTESIAN_POINT ( 'NONE',  ( -20.33245250387252767, 4.503473919074798104, -1.500000000000002220 ) ) ;
#14737=CARTESIAN_POINT ( 'NONE',  ( -12.70408864715453667, 17.69581422525067183, 11.49999999999999645 ) ) ;
#14738=CARTESIAN_POINT ( 'NONE',  ( -100.4326965455115044, -25.18492896333868103, 3.293943116708551777 ) ) ;
#14739=CARTESIAN_POINT ( 'NONE',  ( -78.64730139296283085, -23.48786465467241058, 11.44779295918254469 ) ) ;
#14740=CARTESIAN_POINT ( 'NONE',  ( -15.54266751046811557, -16.22994250641250957, -1.500000000000002220 ) ) ;
#14741=B_SPLINE_CURVE_WITH_KNOTS ( 'NONE', 3,
 ( #67366, #20173, #12566, #14050 ),
 .UNSPECIFIED., .F., .F.,
 ( 4, 4 ),
 ( 2.186341471430182952E-11, 0.0004637143556766918197 ),
 .UNSPECIFIED. ) ;
#14742=CARTESIAN_POINT ( 'NONE',  ( -50.64790834543075704, -25.26334744936552212, 4.705120468826944347 ) ) ;
#14743=ORIENTED_EDGE ( 'NONE', *, *, #33752, .T. ) ;
#14745=CARTESIAN_POINT ( 'NONE',  ( -38.52287095715006870, -23.47596703998600631, 11.44779298504229281 ) ) ;
#14747=ORIENTED_EDGE ( 'NONE', *, *, #60450, .F. ) ;
#14749=CARTESIAN_POINT ( 'NONE',  ( -46.55318986248427393, -23.96169478059712432, 10.65365249895718414 ) ) ;
#14750=VERTEX_POINT ( 'NONE', #66417 ) ;
#14751=CARTESIAN_POINT ( 'NONE',  ( -0.3244385709253747585, -21.36021439428519386, -1.500000000000002220 ) ) ;
#14752=ORIENTED_EDGE ( 'NONE', *, *, #59234, .T. ) ;
#14753=CARTESIAN_POINT ( 'NONE',  ( -18.19455084753484542, -10.52586660885228298, -1.500000000000002220 ) ) ;
#14754=DIRECTION ( 'NONE',  ( 0.000000000000000000, 0.9999999999976377785, 2.173523156925979128E-06 ) ) ;
#14756=CARTESIAN_POINT ( 'NONE',  ( -1.351711525931510449, 21.94731587555429186, -1.500000000000002220 ) ) ;
#14757=CARTESIAN_POINT ( 'NONE',  ( -87.64316148452599009, -23.48783264082478084, -1.443836473390063713 ) ) ;
#14758=VERTEX_POINT ( 'NONE', #50670 ) ;
#14760=EDGE_CURVE ( 'NONE', #86370, #18719, #45481, .T. ) ;
#14762=FACE_OUTER_BOUND ( 'NONE', #52222, .T. ) ;
#14764=CARTESIAN_POINT ( 'NONE',  ( -127.2228709571500360, -23.47596703998600631, 11.44779298504227860 ) ) ;
#14766=CARTESIAN_POINT ( 'NONE',  ( -20.42270456864569184, -23.87886260247287495, 8.909134979017293787 ) ) ;
#14767=CARTESIAN_POINT ( 'NONE',  ( -4.730540317195566224, 20.75322969461001676, 11.49999999999998934 ) ) ;
#14768=DIRECTION ( 'NONE',  ( -3.773278334444167608E-23, 1.000000000000000000, 0.000000000000000000 ) ) ;
#14769=CARTESIAN_POINT ( 'NONE',  ( -100.4381051993576506, -29.50248914370730091, 2.832395270851967073 ) ) ;
#14771=LINE ( 'NONE', #53857, #50296 ) ;
#14772=CARTESIAN_POINT ( 'NONE',  ( -85.62287095715009855, -24.62285846362214059, 9.038163152653529764 ) ) ;
#14773=CARTESIAN_POINT ( 'NONE',  ( 15.74396088501716839, 16.14010210793005839, -1.500000000000002220 ) ) ;
#14776=CARTESIAN_POINT ( 'NONE',  ( -101.3738023147422780, -25.27307239909452008, 3.986250617436227550 ) ) ;
#14779=CARTESIAN_POINT ( 'NONE',  ( -10.75157073690095721, 16.42123490324765811, 11.49999999999999645 ) ) ;
#14782=ORIENTED_EDGE ( 'NONE', *, *, #90005, .F. ) ;
#14783=B_SPLINE_CURVE_WITH_KNOTS ( 'NONE', 3,
 ( #38880, #78935, #69842, #46501 ),
 .UNSPECIFIED., .F., .F.,
 ( 4, 4 ),
 ( 0.7693278071035449805, 0.7703285541443105622 ),
 .UNSPECIFIED. ) ;
#14784=CARTESIAN_POINT ( 'NONE',  ( -88.63863195549789964, -23.73791477778912196, 11.05961554403170588 ) ) ;
#14785=CARTESIAN_POINT ( 'NONE',  ( -125.5800465235194849, -25.31863276151772979, 6.461862851402581320 ) ) ;
#14786=CARTESIAN_POINT ( 'NONE',  ( -124.5891619642989525, -24.51419770103158768, 9.386484678747164523 ) ) ;
#14787=CARTESIAN_POINT ( 'NONE',  ( 7.987771016649366729, -18.01272016045900415, -1.500000000000002220 ) ) ;
#14788=ORIENTED_EDGE ( 'NONE', *, *, #25488, .T. ) ;
#14791=EDGE_CURVE ( 'NONE', #90885, #13954, #49076, .T. ) ;
#14792=EDGE_CURVE ( 'NONE', #24496, #94960, #66906, .T. ) ;
#14796=DIRECTION ( 'NONE',  ( -3.773278334453079618E-23, 0.9999999999976377785, 2.173523156925979975E-06 ) ) ;
#14797=CARTESIAN_POINT ( 'NONE',  ( -55.53718012664960924, -24.63355581998386157, 0.9682620441943822209 ) ) ;
#14798=CARTESIAN_POINT ( 'NONE',  ( -100.0332803147414324, -25.03145169341005527, 7.519340699400126837 ) ) ;
#14801=CARTESIAN_POINT ( 'NONE',  ( -43.55620429048338593, -23.48786465467240347, 11.44779295918255180 ) ) ;
#14802=CARTESIAN_POINT ( 'NONE',  ( -19.26508835251014773, 5.270845654819066084, -1.500000000000002220 ) ) ;
#14804=CARTESIAN_POINT ( 'NONE',  ( -45.50996254517149708, -23.85049219812685095, 10.88485053497527133 ) ) ;
#14805=ORIENTED_EDGE ( 'NONE', *, *, #61577, .F. ) ;
#14808=CARTESIAN_POINT ( 'NONE',  ( -66.52287095715009002, -24.34917612406836795, 0.1852690917426535466 ) ) ;
#14809=CARTESIAN_POINT ( 'NONE',  ( -80.59639368748227639, -24.15602025860896163, 10.28564288303536145 ) ) ;
#14810=CARTESIAN_POINT ( 'NONE',  ( -120.6228709571500559, -24.15431212366390668, -0.2830839119428921191 ) ) ;
#14811=CARTESIAN_POINT ( 'NONE',  ( -39.48568060755304288, -24.51314013834315730, 0.6176544820404118452 ) ) ;
#14812=B_SPLINE_CURVE_WITH_KNOTS ( 'NONE', 3,
 ( #25972, #25468, #56444, #17864, #78737, #94481 ),
 .UNSPECIFIED., .F., .F.,
 ( 4, 2, 4 ),
 ( 0.000000000000000000, 0.001380901958385384858, 0.002761803916770769717 ),
 .UNSPECIFIED. ) ;
#14814=CARTESIAN_POINT ( 'NONE',  ( -27.75512989467660674, -25.26026286428627188, 1.629582517731039459 ) ) ;
#14816=DIRECTION ( 'NONE',  ( -3.773278334453079030E-23, 0.9999999999976377785, 2.173523156925979128E-06 ) ) ;
#14817=CARTESIAN_POINT ( 'NONE',  ( -89.62287095715004170, -24.66019654487199020, 8.947790411086128159 ) ) ;
#14820=CARTESIAN_POINT ( 'NONE',  ( -5.286950244708777724, -19.55949958832428948, -1.500000000000002220 ) ) ;
#14821=ADVANCED_FACE ( 'NONE', ( #67902 ), #98823, .T. ) ;
#14822=CARTESIAN_POINT ( 'NONE',  ( -76.62287095715004170, -24.51387760970723662, 9.387446482453412955 ) ) ;
#14823=CARTESIAN_POINT ( 'NONE',  ( -109.6228709571500559, -29.50248528299804818, 1.056150453629043584 ) ) ;
#14824=CARTESIAN_POINT ( 'NONE',  ( -83.55620429048339304, -23.48783264082478439, -1.443836473390066377 ) ) ;
#14828=CARTESIAN_POINT ( 'NONE',  ( 0.3675393366473880818, 20.13074986235200470, -1.500000000000002220 ) ) ;
#14829=CARTESIAN_POINT ( 'NONE',  ( -19.97109070424261645, 6.737033823242594366, 11.49999999999999645 ) ) ;
#14831=LINE ( 'NONE', #83854, #2869 ) ;
#14832=CARTESIAN_POINT ( 'NONE',  ( 6.025212951983072607, -21.27585971943098642, -1.500000000000002220 ) ) ;
#14834=CARTESIAN_POINT ( 'NONE',  ( -10.66544979547405347, 17.54311462378693420, -1.500000000000002220 ) ) ;
#14835=CARTESIAN_POINT ( 'NONE',  ( -96.52287095715007581, -23.72747288104470798, -1.053458166803225904 ) ) ;
#14836=CARTESIAN_POINT ( 'NONE',  ( -60.61726270389971205, -23.48783264082476308, -1.443836473390097686 ) ) ;
#14837=ORIENTED_EDGE ( 'NONE', *, *, #46233, .F. ) ;
#14839=ORIENTED_EDGE ( 'NONE', *, *, #9450, .F. ) ;
#14842=CARTESIAN_POINT ( 'NONE',  ( -64.52287095715006160, -24.64965694238407323, 8.947790433994201820 ) ) ;
#14843=VERTEX_POINT ( 'NONE', #30822 ) ;
#14844=VERTEX_POINT ( 'NONE', #37932 ) ;
#14846=DIRECTION ( 'NONE',  ( 3.773278334444166432E-23, -1.000000000000000000, 0.000000000000000000 ) ) ;
#14848=CARTESIAN_POINT ( 'NONE',  ( -68.54058893247888307, -24.51419770103157347, 9.386484678747180510 ) ) ;
#14849=CARTESIAN_POINT ( 'NONE',  ( -18.09956831669839872, 9.893135806712603397, -1.500000000000002220 ) ) ;
#14850=EDGE_CURVE ( 'NONE', #63555, #24333, #9158, .T. ) ;
#14851=CARTESIAN_POINT ( 'NONE',  ( -21.62496174240652991, 0.2022338437372764308, 11.49999999999999645 ) ) ;
#14852=VERTEX_POINT ( 'NONE', #91705 ) ;
#14853=CARTESIAN_POINT ( 'NONE',  ( -81.52287095715001897, -24.66019654487199375, 8.947790411086126383 ) ) ;
#14854=CARTESIAN_POINT ( 'NONE',  ( -57.62287095715006302, -23.95044443724992433, 10.65354141964650125 ) ) ;
#14855=CARTESIAN_POINT ( 'NONE',  ( -21.16225983376422448, 7.283793490815352989, -1.500000000000002220 ) ) ;
#14857=CARTESIAN_POINT ( 'NONE',  ( -62.52287095715006160, -24.65952944569304606, 1.056160979905695463 ) ) ;
#14858=DIRECTION ( 'NONE',  ( 1.000000000000000000, 3.773278334444167608E-23, 8.201307833595939069E-29 ) ) ;
#14859=ORIENTED_EDGE ( 'NONE', *, *, #38995, .F. ) ;
#14861=CARTESIAN_POINT ( 'NONE',  ( -49.60653733798429244, -23.73791477778911840, 11.05961554403170943 ) ) ;
#14863=CARTESIAN_POINT ( 'NONE',  ( -20.92377055399060737, -0.003182555231893603818, 11.49999999999998934 ) ) ;
#14864=ORIENTED_EDGE ( 'NONE', *, *, #50802, .T. ) ;
#14865=CARTESIAN_POINT ( 'NONE',  ( -67.65234729852470252, -23.48786465467241058, 11.44779295918254824 ) ) ;
#14869=PLANE ( 'NONE',  #50338 ) ;
#14870=CARTESIAN_POINT ( 'NONE',  ( 13.39648796734645231, 16.42122281929413319, -1.500000000000002220 ) ) ;
#14871=ORIENTED_EDGE ( 'NONE', *, *, #61127, .T. ) ;
#14873=CARTESIAN_POINT ( 'NONE',  ( -100.4005007646339891, -25.12215675090913081, 7.100843682671821533 ) ) ;
#14874=CARTESIAN_POINT ( 'NONE',  ( 4.771108217193557266, 21.26182814020628697, -1.500000000000002220 ) ) ;
#14875=CARTESIAN_POINT ( 'NONE',  ( -56.62287095715005592, -24.64965695001468404, 8.947790433994185832 ) ) ;
#14876=FACE_OUTER_BOUND ( 'NONE', #16854, .T. ) ;
#14877=B_SPLINE_CURVE_WITH_KNOTS ( 'NONE', 3,
 ( #39418, #93693, #854, #31808, #24677, #4228 ),
 .UNSPECIFIED., .F., .F.,
 ( 4, 2, 4 ),
 ( 0.000000000000000000, 0.001380764517854760195, 0.002761529035709520390 ),
 .UNSPECIFIED. ) ;
#14879=CARTESIAN_POINT ( 'NONE',  ( -5.042499505632127565, 21.24692939306837758, -1.500000000000002220 ) ) ;
#14880=CARTESIAN_POINT ( 'NONE',  ( -78.94548380723361447, -25.26800482900744527, 6.082637674949305406 ) ) ;
#14881=VERTEX_POINT ( 'NONE', #45559 ) ;
#14882=PLANE ( 'NONE',  #63179 ) ;
#14884=CARTESIAN_POINT ( 'NONE',  ( -43.62287095715004881, -24.50216790748099527, 0.6166512839513605959 ) ) ;
#14886=ORIENTED_EDGE ( 'NONE', *, *, #59191, .F. ) ;
#14889=CARTESIAN_POINT ( 'NONE',  ( -44.62287095715004881, -23.47593901973091235, -1.443836447539011525 ) ) ;
#14890=CARTESIAN_POINT ( 'NONE',  ( 15.74494995282791088, 14.18698661492608615, -1.500000000000002220 ) ) ;
#14891=CARTESIAN_POINT ( 'NONE',  ( -94.62287095715009855, -23.96127896941632685, -0.6493128931037828178 ) ) ;
#14892=CARTESIAN_POINT ( 'NONE',  ( -95.62287095714997065, -24.82576562982392332, 8.398263435472967942 ) ) ;
#14896=DIRECTION ( 'NONE',  ( 0.000000000000000000, -0.9999999999976377785, -2.173523156925979975E-06 ) ) ;
#14897=CARTESIAN_POINT ( 'NONE',  ( -51.49344744762370851, -25.31373635202942296, 5.229250005650915689 ) ) ;
#14899=CARTESIAN_POINT ( 'NONE',  ( 17.65527434030279252, -8.155491144718855168, 11.49999999999999645 ) ) ;
#14901=ORIENTED_EDGE ( 'NONE', *, *, #52752, .T. ) ;
#14902=CARTESIAN_POINT ( 'NONE',  ( -113.6228709571500559, -24.64965695001469115, 8.947790433994176951 ) ) ;
#14903=DIRECTION ( 'NONE',  ( 0.000000000000000000, 2.173523156925980399E-06, -0.9999999999976378895 ) ) ;
#14906=CARTESIAN_POINT ( 'NONE',  ( -34.62287095715005592, -23.48786465467240347, 11.44779295918255535 ) ) ;
#14907=CARTESIAN_POINT ( 'NONE',  ( -19.13235715846047214, 4.354950445902704637, 11.49999999999998934 ) ) ;
#14908=DIRECTION ( 'NONE',  ( -3.773278334453079030E-23, 0.9999999999976377785, 2.173523156925979128E-06 ) ) ;
#14911=CARTESIAN_POINT ( 'NONE',  ( 13.05104812959431548, -17.15854754814989391, 11.49999999999998934 ) ) ;
#14913=CARTESIAN_POINT ( 'NONE',  ( -73.62287095715005592, -23.47593901973091235, -1.443836447539006196 ) ) ;
#14914=CARTESIAN_POINT ( 'NONE',  ( -65.58953762381672448, -25.00182538069145721, 7.747789668545095765 ) ) ;
#14915=CARTESIAN_POINT ( 'NONE',  ( 21.10734164270438029, -9.282589649079691085, -1.500000000000002220 ) ) ;
#14916=EDGE_CURVE ( 'NONE', #38339, #82766, #98639, .T. ) ;
#14919=CARTESIAN_POINT ( 'NONE',  ( -94.62287095715005592, -29.50247984919015209, -1.443849546365051806 ) ) ;
#14920=CARTESIAN_POINT ( 'NONE',  ( 11.17094659993960803, -16.83544227557131023, 11.49999999999999645 ) ) ;
#14921=CARTESIAN_POINT ( 'NONE',  ( -121.5915921659258743, -23.73791477778912196, 11.05961554403169878 ) ) ;
#14922=CARTESIAN_POINT ( 'NONE',  ( -64.62287095715002749, -23.96177878511307568, 10.65340807706330217 ) ) ;
#14923=CARTESIAN_POINT ( 'NONE',  ( -109.3584176993576591, -25.27948031066536672, 4.206202526585778756 ) ) ;
#14924=DIRECTION ( 'NONE',  ( 3.773278334444166432E-23, -1.000000000000000000, 0.000000000000000000 ) ) ;
#14925=CARTESIAN_POINT ( 'NONE',  ( -110.4389802415574309, -25.18425583253951672, 3.296667852188002623 ) ) ;
#14926=CARTESIAN_POINT ( 'NONE',  ( 9.006517291608927778, -17.75031788249398446, -1.500000000000002220 ) ) ;
#14928=ADVANCED_FACE ( 'NONE', ( #77479 ), #38930, .T. ) ;
#14929=CARTESIAN_POINT ( 'NONE',  ( -17.81549539028256746, -8.563599010019245839, -1.500000000000002220 ) ) ;
#14931=CARTESIAN_POINT ( 'NONE',  ( -56.53763200549867207, -24.51314013834315730, 0.6176544820404098468 ) ) ;
#14934=DIRECTION ( 'NONE',  ( 3.773278334444167608E-23, -1.000000000000000000, 0.000000000000000000 ) ) ;
#14935=B_SPLINE_CURVE_WITH_KNOTS ( 'NONE', 3,
 ( #85665, #11417, #42392, #17150, #78030, #8542 ),
 .UNSPECIFIED., .F., .F.,
 ( 4, 2, 4 ),
 ( 0.000000000000000000, 0.001380901958385387027, 0.002761803916770774053 ),
 .UNSPECIFIED. ) ;
#14936=CARTESIAN_POINT ( 'NONE',  ( -42.52287095715007581, -24.33832256527049154, 0.1851278514138574860 ) ) ;
#14937=CARTESIAN_POINT ( 'NONE',  ( -9.011640028862021978, 18.61544202926687674, 11.49999999999999645 ) ) ;
#14939=CARTESIAN_POINT ( 'NONE',  ( -50.37830952628071657, -25.25138672683397800, 5.197789126111715063 ) ) ;
#14940=CARTESIAN_POINT ( 'NONE',  ( 2.290073164716609710, 22.57640404599860418, 11.49999999999999645 ) ) ;
#14943=B_SPLINE_SURFACE_WITH_KNOTS ( 'NONE', 3, 1, ( 
 ( #96231, #97224 ),
 ( #58662, #64810 ),
 ( #2893, #33823 ),
 ( #89610, #19089 ),
 ( #34829, #26713 ),
 ( #57674, #95724 ),
 ( #50060, #11481 ),
 ( #73395, #3891 ),
 ( #65799, #96716 ),
 ( #27217, #75867 ),
 ( #75368, #6863 ),
 ( #28209, #21084 ),
 ( #52050, #37815 ),
 ( #68770, #36325 ),
 ( #14464, #21574 ),
 ( #61174, #13471 ),
 ( #60672, #99687 ),
 ( #20586, #45446 ),
 ( #14967, #30192 ),
 ( #91100, #28713 ),
 ( #83481, #38305 ),
 ( #67284, #76360 ),
 ( #29702, #6369 ) ),
 .UNSPECIFIED., .F., .F., .F.,
 ( 4, 1, 1, 1, 1, 1, 1, 1, 1, 1, 1, 1, 1, 1, 1, 1, 1, 1, 1, 1, 4 ),
 ( 2, 2 ),
 ( 0.000000000000000000, 0.07295106587586651370, 0.1415836941865448451, 0.2059264601708667708, 0.2653013571846051799, 0.3205972327139279821, 0.3718165030988102027, 0.4187897697094515315, 0.4616987286157640535, 0.5021335821035650682, 0.5408043152926476083, 0.5781805253279657109, 0.6142968652075138092, 0.6496782432647868477, 0.6842994600896368240, 0.7183589527723606150, 0.7520808646475963810, 0.8176524386023842350, 0.8797220764054374254, 0.9399655597309863886, 1.000000000000000000 ),
 ( 0.000000000000000000, 1.000000000000000000 ),
 .UNSPECIFIED. ) ;
#14944=CARTESIAN_POINT ( 'NONE',  ( -67.52287095715006160, -24.33832256527049154, 0.1851278514138614828 ) ) ;
#14945=CARTESIAN_POINT ( 'NONE',  ( -74.62287095715005592, -24.35013146730203815, 9.818937971375111928 ) ) ;
#14946=CARTESIAN_POINT ( 'NONE',  ( 18.63370447891095694, 7.782165041754079304, 11.49999999999998934 ) ) ;
#14947=EDGE_CURVE ( 'NONE', #20637, #42580, #24697, .T. ) ;
#14949=CARTESIAN_POINT ( 'NONE',  ( -95.62287095715008434, -24.91544648472619983, 1.928969306349227475 ) ) ;
#14950=VERTEX_POINT ( 'NONE', #64807 ) ;
#14951=ORIENTED_EDGE ( 'NONE', *, *, #42293, .T. ) ;
#14952=EDGE_CURVE ( 'NONE', #70257, #17515, #91446, .T. ) ;
#14954=CARTESIAN_POINT ( 'NONE',  ( 19.54225192528841859, -11.95493969655435151, -1.500000000000002220 ) ) ;
#14955=CARTESIAN_POINT ( 'NONE',  ( -40.89256867414531627, -25.13235034710942273, 2.898563804593949023 ) ) ;
#14956=CARTESIAN_POINT ( 'NONE',  ( -14.23256820581467785, 16.29125061305494526, -1.500000000000002220 ) ) ;
#14958=CARTESIAN_POINT ( 'NONE',  ( -34.60129100296713744, -23.96119346886880663, -0.6495511937831990323 ) ) ;
#14960=CARTESIAN_POINT ( 'NONE',  ( -20.67734376658059858, -3.193854526364364954, 11.49999999999999645 ) ) ;
#14962=CARTESIAN_POINT ( 'NONE',  ( -69.42561217104606897, -25.31612484405095387, 5.145891826979088535 ) ) ;
#14964=CARTESIAN_POINT ( 'NONE',  ( -21.70078857174656761, -3.768841730229552045, 11.49999999999998934 ) ) ;
#14965=ADVANCED_FACE ( 'NONE', ( #41951 ), #96229, .F. ) ;
#14966=CARTESIAN_POINT ( 'NONE',  ( -105.6251633804084804, -24.83644354573579349, 8.397322867130096569 ) ) ;
#14967=CARTESIAN_POINT ( 'NONE',  ( -28.29841854899664710, -25.21724961408747845, 7.453534148297638495 ) ) ;
#14968=ORIENTED_EDGE ( 'NONE', *, *, #87977, .T. ) ;
#14971=VERTEX_POINT ( 'NONE', #18585 ) ;
#14972=CARTESIAN_POINT ( 'NONE',  ( -72.55911193603030540, -23.73791477778911840, 11.05961554403170943 ) ) ;
#14973=ORIENTED_EDGE ( 'NONE', *, *, #50259, .F. ) ;
#14975=CARTESIAN_POINT ( 'NONE',  ( -61.64687923781921342, -25.18035200424451858, 3.255061677420811428 ) ) ;
#14976=CARTESIAN_POINT ( 'NONE',  ( -101.4571681947234083, -25.10935903412801906, 3.296845841340303451 ) ) ;
#14978=CARTESIAN_POINT ( 'NONE',  ( -20.16212974941129588, 3.559051167911782887, -1.500000000000002220 ) ) ;
#14979=EDGE_CURVE ( 'NONE', #57577, #71190, #18858, .T. ) ;
#14980=B_SPLINE_CURVE_WITH_KNOTS ( 'NONE', 3,
 ( #16532, #63241, #61742, #47508, #70340, #94163 ),
 .UNSPECIFIED., .F., .F.,
 ( 4, 2, 4 ),
 ( 0.000000000000000000, 0.001380901958385383340, 0.002761803916770766681 ),
 .UNSPECIFIED. ) ;
#14985=CARTESIAN_POINT ( 'NONE',  ( 6.212073114426278408, 21.40951068830820958, -1.500000000000002220 ) ) ;
#14986=EDGE_CURVE ( 'NONE', #73864, #61563, #56682, .T. ) ;
#14987=VECTOR ( 'NONE', #12788, 1000.000000000000114 ) ;
#14989=CARTESIAN_POINT ( 'NONE',  ( -88.62287095715004170, -23.48786465467241769, 11.44779295918254114 ) ) ;
#14991=CARTESIAN_POINT ( 'NONE',  ( -29.80803119424227177, -25.23992228501141000, 4.571394149977143329 ) ) ;
#14994=CARTESIAN_POINT ( 'NONE',  ( -4.186882374726557110, 20.40937146592452223, 11.49999999999998934 ) ) ;
#14996=CARTESIAN_POINT ( 'NONE',  ( -42.52287095715004739, -24.35013146730202749, 9.818937971375117257 ) ) ;
#14997=EDGE_LOOP ( 'NONE', ( #63003, #6864, #15973, #91273 ) ) ;
#14998=VECTOR ( 'NONE', #1834, 1000.000000000000227 ) ;
#15002=CARTESIAN_POINT ( 'NONE',  ( -80.52287095715006160, -29.50250786944525672, 11.44777988621623521 ) ) ;
#15007=CARTESIAN_POINT ( 'NONE',  ( -33.52287095715006160, -29.50248528299804818, 1.056150453629029817 ) ) ;
#15008=LINE ( 'NONE', #29238, #70802 ) ;
#15009=CARTESIAN_POINT ( 'NONE',  ( 22.09269804725545683, -1.632937629565654580, 11.49999999999999645 ) ) ;
#15012=CARTESIAN_POINT ( 'NONE',  ( -1.322449806865925614, 22.60218017400935864, 11.49999999999998934 ) ) ;
#15013=CARTESIAN_POINT ( 'NONE',  ( -124.5562042904833930, -23.47593901973091235, -1.443836447538997536 ) ) ;
#15014=ORIENTED_EDGE ( 'NONE', *, *, #17155, .F. ) ;
#15016=CARTESIAN_POINT ( 'NONE',  ( -67.62287095715008434, -23.47596703998600276, 11.44779298504227505 ) ) ;
#15017=VECTOR ( 'NONE', #4691, 1000.000000000000114 ) ;
#15018=CARTESIAN_POINT ( 'NONE',  ( 13.10547390533899836, 15.29217475743441312, -1.500000000000002220 ) ) ;
#15020=ORIENTED_EDGE ( 'NONE', *, *, #98126, .F. ) ;
#15022=CARTESIAN_POINT ( 'NONE',  ( 20.54922051473491607, -8.805037660420627077, -1.500000000000002220 ) ) ;
#15024=ORIENTED_EDGE ( 'NONE', *, *, #42237, .F. ) ;
#15025=CARTESIAN_POINT ( 'NONE',  ( -101.5158928754072605, -25.25341126112779122, 6.338294183601393073 ) ) ;
#15027=CARTESIAN_POINT ( 'NONE',  ( -121.6228709571500417, -29.50250243563736774, 8.947779886222134493 ) ) ;
#15028=CARTESIAN_POINT ( 'NONE',  ( -85.62287095715005592, -23.47596703998600631, 11.44779298504227860 ) ) ;
#15029=DIRECTION ( 'NONE',  ( 0.000000000000000000, -2.173523156925979552E-06, 0.9999999999976378895 ) ) ;
#15031=B_SPLINE_CURVE_WITH_KNOTS ( 'NONE', 3,
 ( #99861, #28876, #45114, #5531, #68936, #99375, #76032, #59329 ),
 .UNSPECIFIED., .F., .F.,
 ( 4, 2, 2, 4 ),
 ( -0.001240355328176877226, -0.0002398155169399624007, 0.0007607242942969524250, 0.002761803916770786196 ),
 .UNSPECIFIED. ) ;
#15032=CARTESIAN_POINT ( 'NONE',  ( 19.26631176993168282, 3.279242639417544236, 11.49999999999998934 ) ) ;
#15035=CARTESIAN_POINT ( 'NONE',  ( -18.34654256122676941, -11.15389649534839833, 11.49999999999998934 ) ) ;
#15039=CARTESIAN_POINT ( 'NONE',  ( 0.7049041324096299022, -22.85584899170066109, -1.500000000000002220 ) ) ;
#15041=PLANE ( 'NONE',  #15856 ) ;
#15042=CARTESIAN_POINT ( 'NONE',  ( -127.5895376238167245, -23.47593901973091235, -1.443836447538995760 ) ) ;
#15043=CARTESIAN_POINT ( 'NONE',  ( -19.32702923155483177, -5.217993511516596961, 11.49999999999999645 ) ) ;
#15044=CARTESIAN_POINT ( 'NONE',  ( -79.09669456484505190, -25.31594480037252382, 5.260499919381111944 ) ) ;
#15045=FACE_OUTER_BOUND ( 'NONE', #33845, .T. ) ;
#15046=EDGE_CURVE ( 'NONE', #33754, #63555, #76887, .T. ) ;
#15047=ADVANCED_FACE ( 'NONE', ( #829 ), #40973, .T. ) ;
#15050=ORIENTED_EDGE ( 'NONE', *, *, #1879, .T. ) ;
#15051=CARTESIAN_POINT ( 'NONE',  ( -109.5228709571500758, -24.50216790748205042, 0.6166512839542608315 ) ) ;
#15052=CARTESIAN_POINT ( 'NONE',  ( -115.6228709571500275, -23.85229601348996908, 10.88205029486208275 ) ) ;
#15053=ADVANCED_FACE ( 'NONE', ( #31274 ), #84560, .F. ) ;
#15054=CARTESIAN_POINT ( 'NONE',  ( 16.02445091669267185, 14.69945503153335764, 11.49999999999998934 ) ) ;
#15056=CARTESIAN_POINT ( 'NONE',  ( 11.71876819965036809, 15.69520123712499249, -1.500000000000002220 ) ) ;
#15058=CARTESIAN_POINT ( 'NONE',  ( -113.6228709571500559, -29.50247984919015209, -1.443849546365048253 ) ) ;
#15059=EDGE_CURVE ( 'NONE', #52488, #18110, #32154, .T. ) ;
#15061=CARTESIAN_POINT ( 'NONE',  ( -110.1668890976376360, -25.27925955908359157, 5.541054292275473969 ) ) ;
#15063=CARTESIAN_POINT ( 'NONE',  ( 18.09022303007301247, 14.20294132079179938, -1.500000000000002220 ) ) ;
#15066=CARTESIAN_POINT ( 'NONE',  ( -4.863915844574979275, 19.94883092034378791, 11.49999999999999645 ) ) ;
#15067=CARTESIAN_POINT ( 'NONE',  ( -39.56136241089613748, -25.30385213834873781, 5.536731319770037629 ) ) ;
#15068=CARTESIAN_POINT ( 'NONE',  ( -33.62287095715005592, -29.50247984919015209, -1.443849546365062242 ) ) ;
#15069=B_SPLINE_CURVE_WITH_KNOTS ( 'NONE', 3,
 ( #89992, #35215, #36704, #50943 ),
 .UNSPECIFIED., .F., .F.,
 ( 4, 4 ),
 ( 0.3100072930973782892, 0.3190137243694937119 ),
 .UNSPECIFIED. ) ;
#15070=VECTOR ( 'NONE', #35043, 1000.000000000000114 ) ;
#15071=ORIENTED_EDGE ( 'NONE', *, *, #216, .F. ) ;
#15072=CARTESIAN_POINT ( 'NONE',  ( -62.52287095715009002, -24.33927499327855415, 9.819080762295815390 ) ) ;
#15073=PLANE ( 'NONE',  #25074 ) ;
#15074=CARTESIAN_POINT ( 'NONE',  ( -125.6236347618411031, -24.92592662359561828, 8.075495903018000021 ) ) ;
#15078=CARTESIAN_POINT ( 'NONE',  ( -34.62287095715005592, -29.50250243563736774, 8.947779886222150481 ) ) ;
#15081=CARTESIAN_POINT ( 'NONE',  ( 15.83906049732654608, 16.74391201645830662, 11.49999999999999645 ) ) ;
#15082=CARTESIAN_POINT ( 'NONE',  ( -16.48365427610503886, -15.78576583860491489, 11.49999999999998934 ) ) ;
#15084=B_SPLINE_SURFACE_WITH_KNOTS ( 'NONE', 3, 3, ( 
 ( #1821, #9414, #32257, #64238 ),
 ( #79426, #94149, #18032, #86543 ),
 ( #32757, #94657, #88056, #80437 ),
 ( #17030, #39872, #95162, #96165 ),
 ( #25135, #56118, #87043, #34272 ),
 ( #17534, #41381, #26655, #19029 ),
 ( #87550, #49000, #10926, #72335 ) ),
 .UNSPECIFIED., .F., .F., .F.,
 ( 4, 3, 4 ),
 ( 4, 4 ),
 ( 0.7945040050992235869, 0.8970133687736495665, 0.9995227324480755460 ),
 ( 0.1795396207514014797, 0.1806352327094073451 ),
 .UNSPECIFIED. ) ;
#15087=CARTESIAN_POINT ( 'NONE',  ( 1.585521478320181865, 22.38520322874704149, 11.49999999999999645 ) ) ;
#15089=PLANE ( 'NONE',  #10894 ) ;
#15090=CARTESIAN_POINT ( 'NONE',  ( -21.55542221127511482, -4.010009934288176758, -1.500000000000002220 ) ) ;
#15091=B_SPLINE_CURVE_WITH_KNOTS ( 'NONE', 3,
 ( #8026, #7030, #92757, #22736, #53722, #84651 ),
 .UNSPECIFIED., .F., .F.,
 ( 4, 2, 4 ),
 ( 1.570755371633836552E-05, 0.001396183895866087536, 0.002776660238015836446 ),
 .UNSPECIFIED. ) ;
#15093=B_SPLINE_CURVE_WITH_KNOTS ( 'NONE', 3,
 ( #12611, #81633, #43573, #82128 ),
 .UNSPECIFIED., .F., .F.,
 ( 4, 4 ),
 ( 0.3890439316126428348, 0.3900446786534081389 ),
 .UNSPECIFIED. ) ;
#15094=CARTESIAN_POINT ( 'NONE',  ( -87.58323056378104354, -24.66019654487200441, 8.947790411086112172 ) ) ;
#15095=CARTESIAN_POINT ( 'NONE',  ( -33.52287095715006160, -24.66019654487198665, 8.947790411086131712 ) ) ;
#15096=CARTESIAN_POINT ( 'NONE',  ( -48.87380231474225667, -25.25252557466923520, 6.137092008254006359 ) ) ;
#15097=CARTESIAN_POINT ( 'NONE',  ( -117.6228709571500559, -23.47593901973091235, -1.443836447538997536 ) ) ;
#15098=ORIENTED_EDGE ( 'NONE', *, *, #48935, .T. ) ;
#15099=CARTESIAN_POINT ( 'NONE',  ( -11.47117155886032158, -16.94740806926979815, -1.500000000000002220 ) ) ;
#15100=ORIENTED_EDGE ( 'NONE', *, *, #2828, .F. ) ;
#15102=ORIENTED_EDGE ( 'NONE', *, *, #86072, .F. ) ;
#15103=ORIENTED_EDGE ( 'NONE', *, *, #19962, .F. ) ;
#15104=CARTESIAN_POINT ( 'NONE',  ( -22.28253579152010033, 6.022996098971622914, -1.500000000000002220 ) ) ;
#15105=CARTESIAN_POINT ( 'NONE',  ( -41.47729125475370182, -25.30524842186639844, 5.093185296294494790 ) ) ;
#15106=CARTESIAN_POINT ( 'NONE',  ( 19.34776771173714849, 6.126202725962671458, -1.500000000000002220 ) ) ;
#15107=AXIS2_PLACEMENT_3D ( 'NONE', #87514, #63189, #772 ) ;
#15109=CARTESIAN_POINT ( 'NONE',  ( -28.20246834257805091, -25.12682770457861281, 5.848370260082334404 ) ) ;
#15110=FACE_OUTER_BOUND ( 'NONE', #12491, .T. ) ;
#15111=EDGE_CURVE ( 'NONE', #64856, #98355, #93800, .T. ) ;
#15112=CARTESIAN_POINT ( 'NONE',  ( -28.52287095715005805, -23.31185441368106126, 11.44779303854528685 ) ) ;
#15113=CARTESIAN_POINT ( 'NONE',  ( -99.63196111833542545, -23.96169478059713498, 10.65365249895717703 ) ) ;
#15114=CARTESIAN_POINT ( 'NONE',  ( -20.78045986758521835, -5.208592277829342088, 11.49999999999999645 ) ) ;
#15115=ORIENTED_EDGE ( 'NONE', *, *, #59567, .T. ) ;
#15116=CARTESIAN_POINT ( 'NONE',  ( -100.5228709571500758, -23.47593901973090524, -1.443836447538996648 ) ) ;
#15117=CARTESIAN_POINT ( 'NONE',  ( -111.5228709571500616, -23.47593901973090524, -1.443836447538996204 ) ) ;
#15120=CARTESIAN_POINT ( 'NONE',  ( -4.968023186724614959, -20.10795263665959709, 11.49999999999998934 ) ) ;
#15121=EDGE_CURVE ( 'NONE', #94877, #53498, #707, .T. ) ;
#15123=CARTESIAN_POINT ( 'NONE',  ( -123.6228709571500701, -23.96127896941632685, -0.6493128931037793761 ) ) ;
#15126=VERTEX_POINT ( 'NONE', #38886 ) ;
#15129=CARTESIAN_POINT ( 'NONE',  ( -76.52287095715007581, -23.96177878511308634, 10.65340807706329684 ) ) ;
#15130=CARTESIAN_POINT ( 'NONE',  ( 5.197331492371871420, 21.31670716312865466, 11.49999999999999645 ) ) ;
#15132=CARTESIAN_POINT ( 'NONE',  ( 6.619388286264371146, -21.57091762011834390, -1.500000000000002220 ) ) ;
#15133=CARTESIAN_POINT ( 'NONE',  ( -16.09219062524700661, 13.46031615953476468, -1.500000000000002220 ) ) ;
#15135=VECTOR ( 'NONE', #92192, 1000.000000000000114 ) ;
#15136=DIRECTION ( 'NONE',  ( 0.000000000000000000, -2.173523156925980399E-06, 0.9999999999976378895 ) ) ;
#15138=ORIENTED_EDGE ( 'NONE', *, *, #55520, .F. ) ;
#15141=CARTESIAN_POINT ( 'NONE',  ( -5.740839400147730309, 20.75665450205591966, -1.500000000000002220 ) ) ;
#15143=VERTEX_POINT ( 'NONE', #25159 ) ;
#15144=CARTESIAN_POINT ( 'NONE',  ( -20.44436638909326120, 5.324712401148210539, 11.49999999999998934 ) ) ;
#15146=DIRECTION ( 'NONE',  ( -3.773278334453079618E-23, 0.9999999999976377785, 2.173523156925979975E-06 ) ) ;
#15147=DIRECTION ( 'NONE',  ( -1.000000000000000000, -0.000000000000000000, 0.000000000000000000 ) ) ;
#15149=CARTESIAN_POINT ( 'NONE',  ( -73.62287095715005592, -29.50247984919015209, -1.443849546365055359 ) ) ;
#15150=CARTESIAN_POINT ( 'NONE',  ( 19.88262469969689050, -9.776007750257504014, -1.500000000000002220 ) ) ;
#15152=CARTESIAN_POINT ( 'NONE',  ( -71.63518065170222826, -24.15543982623907127, -0.2315651400026636497 ) ) ;
#15153=ORIENTED_EDGE ( 'NONE', *, *, #54147, .T. ) ;
#15154=CARTESIAN_POINT ( 'NONE',  ( -51.88058966555665563, -25.24860181553395932, 5.810524397698039856 ) ) ;
#15157=CARTESIAN_POINT ( 'NONE',  ( -100.6278572774885589, -24.63355581998384380, 0.9682620441943933232 ) ) ;
#15158=CARTESIAN_POINT ( 'NONE',  ( 15.33136405852079243, -11.96835230219363311, 11.49999999999998934 ) ) ;
#15159=CARTESIAN_POINT ( 'NONE',  ( 18.17913347391500523, 11.28257676469832660, -1.500000000000002220 ) ) ;
#15160=CARTESIAN_POINT ( 'NONE',  ( -62.64210508241590958, -23.96119346886881019, -0.6495511937832098015 ) ) ;
#15162=CARTESIAN_POINT ( 'NONE',  ( -79.62287095715001328, -24.51283580621365843, 0.6167428607019644904 ) ) ;
#15163=CARTESIAN_POINT ( 'NONE',  ( -101.3340698065965455, -25.27360105556784475, 3.896482660342662996 ) ) ;
#15164=CARTESIAN_POINT ( 'NONE',  ( -18.45961786539058380, -13.25243217869837231, -1.500000000000002220 ) ) ;
#15165=B_SPLINE_SURFACE_WITH_KNOTS ( 'NONE', 3, 3, ( 
 ( #36958, #73644, #65560, #11732 ),
 ( #19835, #57938, #88877, #57441 ),
 ( #19349, #66056, #50315, #95978 ),
 ( #81251, #67927, #83120, #50812 ),
 ( #95478, #42710, #96976, #56936 ),
 ( #27477, #25964, #72652, #13610 ),
 ( #44578, #75506, #88369, #98847 ) ),
 .UNSPECIFIED., .F., .F., .F.,
 ( 4, 3, 4 ),
 ( 4, 4 ),
 ( 0.0004766839783834271615, 0.1029713700210900945, 0.2054660560637967537 ),
 ( 0.8897203268989763991, 0.8911435667790393866 ),
 .UNSPECIFIED. ) ;
#15166=CARTESIAN_POINT ( 'NONE',  ( -93.52287095715006160, -24.64898659630368272, 1.056161002820827921 ) ) ;
#15167=FACE_OUTER_BOUND ( 'NONE', #46210, .T. ) ;
#15168=CARTESIAN_POINT ( 'NONE',  ( -12.90690225449951001, 15.05119527412115055, 11.49999999999999645 ) ) ;
#15171=VERTEX_POINT ( 'NONE', #42907 ) ;
#15172=CARTESIAN_POINT ( 'NONE',  ( -60.52287095715006870, -24.63287334234176740, 0.9662140553045375224 ) ) ;
#15173=LINE ( 'NONE', #52748, #8555 ) ;
#15177=CARTESIAN_POINT ( 'NONE',  ( 5.966611984012316405, 20.80180421262142687, -1.500000000000002220 ) ) ;
#15178=DIRECTION ( 'NONE',  ( -3.773278334453079618E-23, 0.9999999999976377785, 2.173523156925979975E-06 ) ) ;
#15179=CARTESIAN_POINT ( 'NONE',  ( -10.03281922573575002, -16.61734169602722488, -1.500000000000002220 ) ) ;
#15181=CARTESIAN_POINT ( 'NONE',  ( -79.62287095715005592, -29.50250243563736774, 8.947779886222141599 ) ) ;
#15182=CARTESIAN_POINT ( 'NONE',  ( -48.52287095715006160, -29.50248528299804818, 1.056150453629033370 ) ) ;
#15183=CARTESIAN_POINT ( 'NONE',  ( 8.478510716907816658, 17.93336729499101523, 11.49999999999998934 ) ) ;
#15184=VERTEX_POINT ( 'NONE', #26677 ) ;
#15186=EDGE_CURVE ( 'NONE', #65785, #65683, #2851, .T. ) ;
#15187=CARTESIAN_POINT ( 'NONE',  ( -0.6891947355827284794, 20.32259304938107292, 11.49999999999999645 ) ) ;
#15188=CARTESIAN_POINT ( 'NONE',  ( -80.65304186593860436, -23.48783264082476308, -1.443836473390095687 ) ) ;
#15192=CARTESIAN_POINT ( 'NONE',  ( 0.01195862986790833214, -23.20481386120385636, 3.825958421598584902 ) ) ;
#15193=CARTESIAN_POINT ( 'NONE',  ( -62.58953762381672448, -24.64898659630528854, 1.056161002820822814 ) ) ;
#15194=CARTESIAN_POINT ( 'NONE',  ( -48.88506298778586512, -25.25214647875201379, 5.954471609515935349 ) ) ;
#15195=CARTESIAN_POINT ( 'NONE',  ( -40.50923893080022964, -23.85049219812685095, 10.88485053497527488 ) ) ;
#15197=CARTESIAN_POINT ( 'NONE',  ( -12.91570554291229023, -15.35452705144416896, 11.49999999999998934 ) ) ;
#15198=ADVANCED_FACE ( 'NONE', ( #34292 ), #32780, .T. ) ;
#15200=DIRECTION ( 'NONE',  ( -0.000000000000000000, 2.173523156925979552E-06, -0.9999999999976378895 ) ) ;
#15201=ORIENTED_EDGE ( 'NONE', *, *, #15433, .T. ) ;
#15204=CARTESIAN_POINT ( 'NONE',  ( -14.01358469492184966, -18.07645309290061064, 11.49999999999999645 ) ) ;
#15205=CARTESIAN_POINT ( 'NONE',  ( 15.30562342774392093, -16.77826389816909725, -1.500000000000002220 ) ) ;
#15209=CARTESIAN_POINT ( 'NONE',  ( -38.57582415398436382, -24.66019654487198665, 8.947790411086121054 ) ) ;
#15210=B_SPLINE_CURVE_WITH_KNOTS ( 'NONE', 3,
 ( #4863, #52038, #19077, #74855, #36313, #11471, #98191, #81985, #34318, #42445, #43437, #42939, #51046, #73873, #59661, #19577, #65788, #82476 ),
 .UNSPECIFIED., .F., .F.,
 ( 4, 2, 2, 2, 2, 2, 2, 2, 4 ),
 ( 1.411962612463446054E-17, 0.0004122230507468467478, 0.0006183345761202429895, 0.0008244461014936392855, 0.001030557626867035365, 0.001236669152240431552, 0.001442780677613827956, 0.001545836440300521822, 0.001648892202987215470 ),
 .UNSPECIFIED. ) ;
#15211=PLANE ( 'NONE',  #64381 ) ;
#15213=AXIS2_PLACEMENT_3D ( 'NONE', #82563, #26290, #43020 ) ;
#15216=CARTESIAN_POINT ( 'NONE',  ( -0.9335293527496063559, -20.33857301660709638, 11.49999999999998934 ) ) ;
#15219=EDGE_CURVE ( 'NONE', #91196, #77233, #48522, .T. ) ;
#15220=CARTESIAN_POINT ( 'NONE',  ( -21.12268324108725892, 9.058254180033936009, 11.49999999999998934 ) ) ;
#15221=CARTESIAN_POINT ( 'NONE',  ( -88.52287095715006160, -24.64898659630367916, 1.056161002820827921 ) ) ;
#15223=CARTESIAN_POINT ( 'NONE',  ( -108.5876495711624301, -24.51419770103158768, 9.386484678747162747 ) ) ;
#15224=CARTESIAN_POINT ( 'NONE',  ( -77.62361616268356102, -24.66019654487200441, 8.947790411086108620 ) ) ;
#15225=CARTESIAN_POINT ( 'NONE',  ( -51.59924249663487217, -23.96169478059713143, 10.65365249895718236 ) ) ;
#15226=CARTESIAN_POINT ( 'NONE',  ( -10.85727797829764185, 18.24708236899833835, 11.49999999999999645 ) ) ;
#15227=ORIENTED_EDGE ( 'NONE', *, *, #22285, .T. ) ;
#15229=CARTESIAN_POINT ( 'NONE',  ( -0.9571703918902072505, -22.19477237104690914, 11.49999999999998934 ) ) ;
#15230=CARTESIAN_POINT ( 'NONE',  ( -18.12278953325389708, -9.833843834435361586, -1.500000000000002220 ) ) ;
#15231=ORIENTED_EDGE ( 'NONE', *, *, #70564, .T. ) ;
#15233=CARTESIAN_POINT ( 'NONE',  ( -108.9545715455115129, -25.31627118360455597, 4.170144754312187452 ) ) ;
#15234=EDGE_CURVE ( 'NONE', #12369, #7140, #5566, .T. ) ;
#15236=ORIENTED_EDGE ( 'NONE', *, *, #96905, .F. ) ;
#15237=CARTESIAN_POINT ( 'NONE',  ( -91.55469558775585881, -23.96119346886880663, -0.6495511937832073590 ) ) ;
#15240=CARTESIAN_POINT ( 'NONE',  ( -44.52287095715006160, -23.47593901973090169, -1.443836447538997092 ) ) ;
#15241=CARTESIAN_POINT ( 'NONE',  ( 3.748101851616784774, 20.49759516964078188, -1.500000000000002220 ) ) ;
#15242=CARTESIAN_POINT ( 'NONE',  ( -7.892909027492730267, -20.28523913882780505, 11.49999999999999645 ) ) ;
#15244=CARTESIAN_POINT ( 'NONE',  ( -102.6228709571500417, -23.48786465467241769, 11.44779295918253936 ) ) ;
#15245=CARTESIAN_POINT ( 'NONE',  ( -78.60557720441329366, -23.48786465467241058, 11.44779295918254469 ) ) ;
#15246=CARTESIAN_POINT ( 'NONE',  ( -21.66288588771858770, -5.991481186202806342, 11.49999999999998934 ) ) ;
#15247=CARTESIAN_POINT ( 'NONE',  ( -118.6241804900995191, -24.51419770103160189, 9.386484678747168076 ) ) ;
#15250=CARTESIAN_POINT ( 'NONE',  ( -69.52287095715006160, -23.47596703998600631, 11.44779298504228748 ) ) ;
#15251=B_SPLINE_CURVE_WITH_KNOTS ( 'NONE', 3,
 ( #66448, #96368, #57825, #90752 ),
 .UNSPECIFIED., .F., .F.,
 ( 4, 4 ),
 ( 1.387778780781445521E-17, 9.999999999997510880E-05 ),
 .UNSPECIFIED. ) ;
#15252=VECTOR ( 'NONE', #84355, 1000.000000000000114 ) ;
#15256=ORIENTED_EDGE ( 'NONE', *, *, #29467, .T. ) ;
#15257=CARTESIAN_POINT ( 'NONE',  ( -13.37813101364405100, 16.61575060780308277, -1.500000000000002220 ) ) ;
#15258=ORIENTED_EDGE ( 'NONE', *, *, #77612, .T. ) ;
#15259=CARTESIAN_POINT ( 'NONE',  ( -20.11743356864677423, -6.099313207006018089, -1.500000000000002220 ) ) ;
#15260=CARTESIAN_POINT ( 'NONE',  ( -30.51821544575032519, -25.31106951508110825, 3.857144010898052588 ) ) ;
#15261=CARTESIAN_POINT ( 'NONE',  ( -110.6087918725420423, -25.19910796341628156, 3.322910391071347114 ) ) ;
#15262=CARTESIAN_POINT ( 'NONE',  ( -79.11611000704996854, -25.13069340115296058, 2.947789388436138580 ) ) ;
#15263=CARTESIAN_POINT ( 'NONE',  ( -18.59763704738199408, -11.70098744416181979, -1.500000000000002220 ) ) ;
#15264=CARTESIAN_POINT ( 'NONE',  ( -36.52287095715006870, -23.47593901973090169, -1.443836447538997314 ) ) ;
#15266=FACE_OUTER_BOUND ( 'NONE', #12621, .T. ) ;
#15270=CARTESIAN_POINT ( 'NONE',  ( -20.41428188797595311, -24.04316117960158650, 8.370978854367628230 ) ) ;
#15271=CARTESIAN_POINT ( 'NONE',  ( -15.80959461918071618, 14.24510877297761446, 11.49999999999998934 ) ) ;
#15272=CARTESIAN_POINT ( 'NONE',  ( -31.24388727629350626, -25.30412371111346204, 3.891793866089567455 ) ) ;
#15274=FACE_OUTER_BOUND ( 'NONE', #83079, .T. ) ;
#15275=CARTESIAN_POINT ( 'NONE',  ( -29.52287095715006870, -23.40099448348795264, -1.443836171194820883 ) ) ;
#15276=CARTESIAN_POINT ( 'NONE',  ( 9.939345090160914609, -20.19931669485651682, -1.500000000000002220 ) ) ;
#15277=CARTESIAN_POINT ( 'NONE',  ( -111.9718182513300775, -25.21970293610405633, 6.713732480141158199 ) ) ;
#15279=CARTESIAN_POINT ( 'NONE',  ( -51.05357089062000853, -25.31022451930674677, 5.374527235766375810 ) ) ;
#15280=CARTESIAN_POINT ( 'NONE',  ( -3.586273028688536257, -19.27814873881845514, 11.49999999999999645 ) ) ;
#15281=DIRECTION ( 'NONE',  ( 0.000000000000000000, -0.9999999999976377785, -2.173523156925979975E-06 ) ) ;
#15282=CARTESIAN_POINT ( 'NONE',  ( -76.62287095715007013, -24.64965695001468404, 8.947790433994182280 ) ) ;
#15283=B_SPLINE_CURVE_WITH_KNOTS ( 'NONE', 3,
 ( #58509, #50891, #98036, #80837 ),
 .UNSPECIFIED., .F., .F.,
 ( 4, 4 ),
 ( 0.7403145649873383860, 0.7493209962594540308 ),
 .UNSPECIFIED. ) ;
#15286=LINE ( 'NONE', #70087, #93373 ) ;
#15287=CARTESIAN_POINT ( 'NONE',  ( -91.96692758709957616, -25.12049752546737480, 2.832404795212227100 ) ) ;
#15288=CARTESIAN_POINT ( 'NONE',  ( -0.8432318219891272726, -19.69000482574202238, -1.500000000000002220 ) ) ;
#15290=ADVANCED_FACE ( 'NONE', ( #19549 ), #97746, .T. ) ;
#15291=B_SPLINE_CURVE_WITH_KNOTS ( 'NONE', 3,
 ( #32826, #38932, #55180, #40939 ),
 .UNSPECIFIED., .F., .F.,
 ( 4, 4 ),
 ( 0.000000000000000000, 9.999999999998900014E-05 ),
 .UNSPECIFIED. ) ;
#15293=CARTESIAN_POINT ( 'NONE',  ( -118.5228709571501184, -23.73907113216990794, -1.053371485793245244 ) ) ;
#15297=ORIENTED_EDGE ( 'NONE', *, *, #13569, .T. ) ;
#15299=CARTESIAN_POINT ( 'NONE',  ( -39.52287095715006870, -24.64898659630528144, 1.056161002820819261 ) ) ;
#15300=CARTESIAN_POINT ( 'NONE',  ( -55.52645498910460020, -25.00158670708910336, 2.256160236439221034 ) ) ;
#15301=CARTESIAN_POINT ( 'NONE',  ( -86.62287095715004170, -29.50250243563736774, 8.947779886222139822 ) ) ;
#15302=DIRECTION ( 'NONE',  ( 1.000000000000000000, 3.773278334444167608E-23, 8.201307833595939069E-29 ) ) ;
#15303=CARTESIAN_POINT ( 'NONE',  ( -94.55620429048339304, -24.65952944569304961, 1.056160979905701236 ) ) ;
#15305=CARTESIAN_POINT ( 'NONE',  ( -15.89961544564849305, 12.09337254111102844, -1.500000000000002220 ) ) ;
#15306=EDGE_CURVE ( 'NONE', #16795, #73446, #37019, .T. ) ;
#15309=DIRECTION ( 'NONE',  ( -3.773278334453079030E-23, 0.9999999999976377785, 2.173523156925979128E-06 ) ) ;
#15310=ORIENTED_EDGE ( 'NONE', *, *, #71554, .T. ) ;
#15313=CARTESIAN_POINT ( 'NONE',  ( -35.62710011636686147, -23.48783264082477729, -1.443836473390077701 ) ) ;
#15314=CARTESIAN_POINT ( 'NONE',  ( -106.5895376238167387, -23.48786465467241769, 11.44779295918253759 ) ) ;
#15316=CARTESIAN_POINT ( 'NONE',  ( -83.62359966500085307, -24.65952944569305316, 1.056160979905701680 ) ) ;
#15317=CARTESIAN_POINT ( 'NONE',  ( -81.52287095715006160, -23.47596703998600631, 11.44779298504228571 ) ) ;
#15319=ORIENTED_EDGE ( 'NONE', *, *, #79553, .T. ) ;
#15320=CARTESIAN_POINT ( 'NONE',  ( -18.77428246231291808, -7.638711222589018135, 11.49999999999998934 ) ) ;
#15323=CARTESIAN_POINT ( 'NONE',  ( -90.52287095715003318, -24.91544648472626378, 1.928969306349430424 ) ) ;
#15324=ORIENTED_EDGE ( 'NONE', *, *, #2250, .T. ) ;
#15326=EDGE_CURVE ( 'NONE', #87201, #5271, #59849, .T. ) ;
#15327=CARTESIAN_POINT ( 'NONE',  ( 20.05498121024909253, 1.910150955369836812, -1.500000000000002220 ) ) ;
#15328=CARTESIAN_POINT ( 'NONE',  ( 20.99878002148846790, -2.064974809011826729, 11.49999999999999645 ) ) ;
#15330=CARTESIAN_POINT ( 'NONE',  ( -64.55620429048339304, -24.66019654487199020, 8.947790411086133489 ) ) ;
#15331=CARTESIAN_POINT ( 'NONE',  ( 16.06085343747454175, -15.19291221174989204, 11.49999999999998934 ) ) ;
#15333=CARTESIAN_POINT ( 'NONE',  ( 18.81462172601333549, -8.267562025728075525, -1.500000000000002220 ) ) ;
#15334=DIRECTION ( 'NONE',  ( -3.773278334453079030E-23, 0.9999999999976377785, 2.173523156925979128E-06 ) ) ;
#15335=CARTESIAN_POINT ( 'NONE',  ( -60.59908362041784358, -24.15503026093916006, -0.2815557561904390993 ) ) ;
#15337=DIRECTION ( 'NONE',  ( 0.000000000000000000, -0.9999999999976377785, -2.173523156925979128E-06 ) ) ;
#15340=B_SPLINE_SURFACE_WITH_KNOTS ( 'NONE', 3, 1, ( 
 ( #10638, #95869 ),
 ( #65455, #27363 ),
 ( #96372, #88772 ),
 ( #19240, #11626 ),
 ( #5573, #82197 ),
 ( #83185, #44642 ),
 ( #60385, #91800 ),
 ( #22276, #91308 ),
 ( #58874, #89814 ),
 ( #29404, #84187 ),
 ( #53259, #97910 ),
 ( #67484, #14678 ),
 ( #74583, #66998 ),
 ( #59369, #20284 ),
 ( #4591, #44144 ) ),
 .UNSPECIFIED., .F., .F., .F.,
 ( 4, 1, 1, 1, 1, 1, 1, 1, 1, 1, 1, 1, 4 ),
 ( 2, 2 ),
 ( 0.000000000000000000, 0.08940971111013579220, 0.1763057644831058923, 0.2626259021834156937, 0.3494457264756534176, 0.4354982637429541947, 0.5189281301037146354, 0.6013546565787400988, 0.6842564217184154973, 0.7658067397968338907, 0.8448768657103881141, 0.9222797948488744568, 1.000000000000000000 ),
 ( 0.000000000000000000, 1.000000000000000000 ),
 .UNSPECIFIED. ) ;
#15342=VERTEX_POINT ( 'NONE', #90067 ) ;
#15343=ORIENTED_EDGE ( 'NONE', *, *, #23812, .T. ) ;
#15345=ORIENTED_EDGE ( 'NONE', *, *, #12664, .T. ) ;
#15346=CARTESIAN_POINT ( 'NONE',  ( -80.80810375339596874, -25.28533477229251147, 4.196857630783810578 ) ) ;
#15347=CARTESIAN_POINT ( 'NONE',  ( -49.85452831604734314, -25.04816763092740217, 7.491332617951499628 ) ) ;
#15348=CARTESIAN_POINT ( 'NONE',  ( -68.64586005558507509, -23.73791477778911840, 11.05961554403170943 ) ) ;
#15349=CARTESIAN_POINT ( 'NONE',  ( -18.79711486612840332, 8.613068827758688428, -1.500000000000002220 ) ) ;
#15350=CARTESIAN_POINT ( 'NONE',  ( -19.28869470675124731, 9.786980993800005635, 11.49999999999999645 ) ) ;
#15351=ORIENTED_EDGE ( 'NONE', *, *, #53126, .T. ) ;
#15352=PLANE ( 'NONE',  #75841 ) ;
#15354=CARTESIAN_POINT ( 'NONE',  ( -7.019573500991415749, 21.25910006591672996, 11.49999999999998934 ) ) ;
#15355=CARTESIAN_POINT ( 'NONE',  ( -80.15527233487838998, -25.12205802297570401, 7.057878230000818931 ) ) ;
#15356=CARTESIAN_POINT ( 'NONE',  ( -88.62287095715002749, -24.66019654487199730, 8.947790411086128159 ) ) ;
#15358=CARTESIAN_POINT ( 'NONE',  ( -99.61025418334982362, -25.29543586644560094, 4.300707857027740388 ) ) ;
#15360=CARTESIAN_POINT ( 'NONE',  ( -33.52287095715005449, -23.72747288104469732, -1.053458166803227902 ) ) ;
#15361=CARTESIAN_POINT ( 'NONE',  ( -19.40224465947428456, -7.824916089261592766, -1.500000000000002220 ) ) ;
#15364=EDGE_CURVE ( 'NONE', #1762, #12512, #56267, .T. ) ;
#15365=CARTESIAN_POINT ( 'NONE',  ( -67.49333554985891226, -24.66019654487199730, 8.947790411086115725 ) ) ;
#15368=CARTESIAN_POINT ( 'NONE',  ( 19.38521227897113874, -8.589346653930519437, -1.500000000000002220 ) ) ;
#15370=CARTESIAN_POINT ( 'NONE',  ( -50.65952998986089995, -23.85016227208579309, -0.8807180028928346394 ) ) ;
#15372=CARTESIAN_POINT ( 'NONE',  ( 1.472770742059883897, 21.73951962378590963, -1.500000000000002220 ) ) ;
#15373=CARTESIAN_POINT ( 'NONE',  ( -60.58953762381671737, -23.47596703998600276, 11.44779298504227505 ) ) ;
#15374=CARTESIAN_POINT ( 'NONE',  ( -50.62287095715005592, -24.99156045073392463, 7.747789690856161648 ) ) ;
#15375=CARTESIAN_POINT ( 'NONE',  ( -79.57012802947382113, -25.20210771990827325, 6.663789735179169504 ) ) ;
#15376=CARTESIAN_POINT ( 'NONE',  ( -11.22809577558575000, 18.72649003030000259, -1.500000000000002220 ) ) ;
#15377=CARTESIAN_POINT ( 'NONE',  ( -79.12865799501358310, -25.18586200194109281, 6.785185366648832428 ) ) ;
#15378=ORIENTED_EDGE ( 'NONE', *, *, #95265, .F. ) ;
#15379=CARTESIAN_POINT ( 'NONE',  ( -69.62287095715005592, -23.48786465467241058, 11.44779295918254824 ) ) ;
#15380=FACE_OUTER_BOUND ( 'NONE', #86116, .T. ) ;
#15382=VERTEX_POINT ( 'NONE', #82447 ) ;
#15385=ORIENTED_EDGE ( 'NONE', *, *, #65704, .F. ) ;
#15388=B_SPLINE_CURVE_WITH_KNOTS ( 'NONE', 3,
 ( #98496, #83282, #6158, #37111, #98997, #61462 ),
 .UNSPECIFIED., .F., .F.,
 ( 4, 2, 4 ),
 ( 2.780973288783981667E-17, 0.0002696131282151457303, 0.0005392262564302635966 ),
 .UNSPECIFIED. ) ;
#15389=CARTESIAN_POINT ( 'NONE',  ( -19.34623641613454836, -8.721557147202650739, -1.500000000000002220 ) ) ;
#15390=B_SPLINE_CURVE_WITH_KNOTS ( 'NONE', 3,
 ( #60512, #66638, #68606, #82328 ),
 .UNSPECIFIED., .F., .F.,
 ( 4, 4 ),
 ( 0.000000000000000000, 0.0008333333333333595161 ),
 .UNSPECIFIED. ) ;
#15391=CARTESIAN_POINT ( 'NONE',  ( -94.59406255952302445, -23.96119346886881019, -0.6495511937832051386 ) ) ;
#15392=CARTESIAN_POINT ( 'NONE',  ( -78.99318656846928377, -25.27791721166854089, 6.404754622004839248 ) ) ;
#15395=CARTESIAN_POINT ( 'NONE',  ( 3.017506814366913481, 19.14668354085002733, -1.500000000000002220 ) ) ;
#15396=CARTESIAN_POINT ( 'NONE',  ( -69.39739843404061048, -25.28243495002747920, 5.901832878838482621 ) ) ;
#15397=EDGE_LOOP ( 'NONE', ( #65343, #46106, #26759, #83459 ) ) ;
#15398=CARTESIAN_POINT ( 'NONE',  ( 14.64286990871793392, 12.78475832571431070, 11.49999999999999645 ) ) ;
#15399=CARTESIAN_POINT ( 'NONE',  ( -111.6228709571500559, -29.50248528299804818, 1.056150453629043584 ) ) ;
#15400=EDGE_CURVE ( 'NONE', #96024, #7215, #69542, .T. ) ;
#15402=FACE_OUTER_BOUND ( 'NONE', #74020, .T. ) ;
#15403=ORIENTED_EDGE ( 'NONE', *, *, #74440, .T. ) ;
#15406=B_SPLINE_CURVE_WITH_KNOTS ( 'NONE', 3,
 ( #25455, #15960, #246, #84980, #33576, #10741, #49823, #87352, #48813, #77356, #3142, #100180, #62163, #57434, #72148, #79738, #64554, #95471, #25958, #23065, #34083, #95972, #26471, #11236, #42213, #54054 ),
 .UNSPECIFIED., .F., .F.,
 ( 4, 2, 2, 2, 2, 2, 2, 2, 2, 2, 2, 2, 4 ),
 ( 9.172631729222333727E-06, 0.001697682463320513953, 0.002541937379116161830, 0.003386192294911809925, 0.004230447210707458452, 0.005074702126503106113, 0.006763211958094405771, 0.007607466873890056901, 0.008451721789685704561, 0.01014023162127699815, 0.01098448653707264494, 0.01182874145286829173, 0.01351725128445958879 ),
 .UNSPECIFIED. ) ;
#15407=DIRECTION ( 'NONE',  ( 1.000000000000000000, 3.773278334444166432E-23, 8.201307841325785021E-29 ) ) ;
#15408=CARTESIAN_POINT ( 'NONE',  ( -93.58858278818280496, -24.35071581493543391, 9.817618358456016381 ) ) ;
#15409=CARTESIAN_POINT ( 'NONE',  ( -18.74126595726828626, 5.813943427813767606, -1.500000000000002220 ) ) ;
#15410=CARTESIAN_POINT ( 'NONE',  ( -117.6228709571500559, -23.73934037231758154, 11.05740245334328264 ) ) ;
#15411=ORIENTED_EDGE ( 'NONE', *, *, #37567, .F. ) ;
#15412=VECTOR ( 'NONE', #3852, 1000.000000000000114 ) ;
#15413=CARTESIAN_POINT ( 'NONE',  ( 14.45009471711328786, 16.04676183837579373, 11.49999999999998934 ) ) ;
#15415=CARTESIAN_POINT ( 'NONE',  ( -40.53341874850772086, -24.63355581998386512, 0.9682620441943814438 ) ) ;
#15416=CARTESIAN_POINT ( 'NONE',  ( -90.52287095715006160, -23.48786465467241769, 11.44779295918254292 ) ) ;
#15417=CARTESIAN_POINT ( 'NONE',  ( 22.66633601775066253, -4.223608244049824378, -1.500000000000002220 ) ) ;
#15418=EDGE_CURVE ( 'NONE', #67116, #69390, #76691, .T. ) ;
#15419=ADVANCED_FACE ( 'NONE', ( #22524 ), #49098, .T. ) ;
#15421=FACE_OUTER_BOUND ( 'NONE', #77772, .T. ) ;
#15423=CARTESIAN_POINT ( 'NONE',  ( -121.6240024248556040, -24.51419770103157347, 9.386484678747175181 ) ) ;
#15424=CARTESIAN_POINT ( 'NONE',  ( -100.8191360062217399, -25.05035194608113613, 7.529171757875409376 ) ) ;
#15426=CARTESIAN_POINT ( 'NONE',  ( -98.52287095715001897, -23.94994826722565406, -0.6494450866342705853 ) ) ;
#15427=CARTESIAN_POINT ( 'NONE',  ( -114.5873116467302708, -24.66019654487200441, 8.947790411086106843 ) ) ;
#15428=CARTESIAN_POINT ( 'NONE',  ( 7.614665684681447111, -18.39110272641453037, 11.49999999999998934 ) ) ;
#15429=EDGE_CURVE ( 'NONE', #21992, #26463, #54009, .T. ) ;
#15431=CARTESIAN_POINT ( 'NONE',  ( 18.78741845327603599, -6.401996767227196905, -1.500000000000002220 ) ) ;
#15432=CARTESIAN_POINT ( 'NONE',  ( -56.49721973070467129, -24.34968618360933590, 0.1864209137778786995 ) ) ;
#15433=EDGE_CURVE ( 'NONE', #25116, #19170, #92527, .T. ) ;
#15437=CARTESIAN_POINT ( 'NONE',  ( -18.06733440434376092, 10.15830956056102963, 11.49999999999999645 ) ) ;
#15438=CARTESIAN_POINT ( 'NONE',  ( -129.6228709571500417, -29.50250243563736774, 8.947779886222132717 ) ) ;
#15440=CARTESIAN_POINT ( 'NONE',  ( -49.68170153635294639, -25.25138720524621760, 5.417898236803782908 ) ) ;
#15441=CARTESIAN_POINT ( 'NONE',  ( 21.16149768242404861, -8.233860041645145955, 11.49999999999999645 ) ) ;
#15443=B_SPLINE_CURVE_WITH_KNOTS ( 'NONE', 3,
 ( #66284, #59157, #43439, #81987, #4375, #36813 ),
 .UNSPECIFIED., .F., .F.,
 ( 4, 2, 4 ),
 ( 1.570755371633915156E-05, 0.001396183895866085801, 0.002776660238015832543 ),
 .UNSPECIFIED. ) ;
#15444=CARTESIAN_POINT ( 'NONE',  ( -60.62287095715002039, -24.15431212366389602, -0.2830839119429001682 ) ) ;
#15445=CARTESIAN_POINT ( 'NONE',  ( -74.62287095715009855, -23.73934037231756733, 11.05740245334329153 ) ) ;
#15446=CARTESIAN_POINT ( 'NONE',  ( -1.055277534996966970, 20.15608268182561247, 11.49999999999998934 ) ) ;
#15449=CARTESIAN_POINT ( 'NONE',  ( -45.52287095715006160, -23.48786465467240347, 11.44779295918255002 ) ) ;
#15452=VERTEX_POINT ( 'NONE', #69221 ) ;
#15454=CARTESIAN_POINT ( 'NONE',  ( 15.01570752033863165, -17.30494853738164096, 11.49999999999998934 ) ) ;
#15455=CARTESIAN_POINT ( 'NONE',  ( -41.82691350321800172, -25.26045596155741890, 3.841969471408021253 ) ) ;
#15456=CARTESIAN_POINT ( 'NONE',  ( 0.6597851148675514255, -21.60297929554585394, -1.500000000000002220 ) ) ;
#15458=CARTESIAN_POINT ( 'NONE',  ( -69.62287095715005592, -29.50250243563736774, 8.947779886222143375 ) ) ;
#15459=CARTESIAN_POINT ( 'NONE',  ( -2.496121100066326814, 20.73550571027955769, 11.49999999999999645 ) ) ;
#15461=CARTESIAN_POINT ( 'NONE',  ( -124.6246529919008594, -24.15543982623907127, -0.2315651400026562945 ) ) ;
#15462=CARTESIAN_POINT ( 'NONE',  ( -16.14483305390557888, 14.99321182834783528, -1.500000000000002220 ) ) ;
#15464=CARTESIAN_POINT ( 'NONE',  ( -65.62287095715008434, -24.62285846362216191, 9.038163152653529764 ) ) ;
#15465=EDGE_CURVE ( 'NONE', #47759, #5356, #93540, .T. ) ;
#15466=ORIENTED_EDGE ( 'NONE', *, *, #26545, .T. ) ;
#15473=CARTESIAN_POINT ( 'NONE',  ( -41.62287095715006302, -24.64965695001467694, 8.947790433994187609 ) ) ;
#15474=CARTESIAN_POINT ( 'NONE',  ( -101.7453191491394477, -25.27404852088134746, 3.852396047414954339 ) ) ;
#15476=CARTESIAN_POINT ( 'NONE',  ( -20.02755620033356010, -4.236777897013602079, -1.500000000000002220 ) ) ;
#15477=ORIENTED_EDGE ( 'NONE', *, *, #50593, .F. ) ;
#15478=CARTESIAN_POINT ( 'NONE',  ( -110.5228709571500616, -24.99156044556120548, 7.747789690856173195 ) ) ;
#15481=CARTESIAN_POINT ( 'NONE',  ( 18.42719714020066846, 12.55551944762973626, -1.500000000000002220 ) ) ;
#15483=CARTESIAN_POINT ( 'NONE',  ( -91.52287095715006160, -23.47593901973090524, -1.443836447538996648 ) ) ;
#15484=VERTEX_POINT ( 'NONE', #24035 ) ;
#15485=CARTESIAN_POINT ( 'NONE',  ( -29.81175120719462157, -25.24633111994858581, 4.942810988825437235 ) ) ;
#15486=CARTESIAN_POINT ( 'NONE',  ( -39.52287095715004739, -24.51387760970725438, 9.387446482453428942 ) ) ;
#15487=CARTESIAN_POINT ( 'NONE',  ( -17.17656601037699104, 11.78060583124977256, 11.49999999999998934 ) ) ;
#15492=CARTESIAN_POINT ( 'NONE',  ( -51.45055690290539019, -25.12217740856155146, 6.541367195127278045 ) ) ;
#15493=ORIENTED_EDGE ( 'NONE', *, *, #57367, .F. ) ;
#15494=DIRECTION ( 'NONE',  ( 0.000000000000000000, -2.173523156925979552E-06, 0.9999999999976378895 ) ) ;
#15495=CARTESIAN_POINT ( 'NONE',  ( -121.5228709571500616, -23.48786465467241769, 11.44779295918253759 ) ) ;
#15497=DIRECTION ( 'NONE',  ( -3.773278334453079618E-23, 0.9999999999976377785, 2.173523156925979975E-06 ) ) ;
#15499=DIRECTION ( 'NONE',  ( -3.773278334453079618E-23, 0.9999999999976377785, 2.173523156925979975E-06 ) ) ;
#15500=CARTESIAN_POINT ( 'NONE',  ( -5.994446910899359438, -21.39327697068355505, 11.49999999999999645 ) ) ;
#15502=CARTESIAN_POINT ( 'NONE',  ( -38.62287095715005592, -24.34917612406837506, 0.1852690917426539075 ) ) ;
#15503=ORIENTED_EDGE ( 'NONE', *, *, #52988, .T. ) ;
#15504=CARTESIAN_POINT ( 'NONE',  ( 14.74224262856723833, 17.19160420931263999, 11.49999999999998934 ) ) ;
#15505=ADVANCED_FACE ( 'NONE', ( #78317 ), #8823, .F. ) ;
#15507=B_SPLINE_CURVE_WITH_KNOTS ( 'NONE', 3,
 ( #8826, #32153, #1220, #16931 ),
 .UNSPECIFIED., .F., .F.,
 ( 4, 4 ),
 ( 0.000000000000000000, 9.999999999996123101E-05 ),
 .UNSPECIFIED. ) ;
#15510=ORIENTED_EDGE ( 'NONE', *, *, #95148, .F. ) ;
#15511=EDGE_CURVE ( 'NONE', #45688, #54341, #68280, .T. ) ;
#15513=VECTOR ( 'NONE', #60789, 1000.000000000000114 ) ;
#15514=CARTESIAN_POINT ( 'NONE',  ( -19.48533387766964964, -5.011242947278518045, -1.500000000000002220 ) ) ;
#15518=LINE ( 'NONE', #39865, #43906 ) ;
#15519=CARTESIAN_POINT ( 'NONE',  ( 0.3464652362752086434, -22.36268665536068667, -1.500000000000002220 ) ) ;
#15520=EDGE_CURVE ( 'NONE', #85004, #54879, #33152, .T. ) ;
#15522=VERTEX_POINT ( 'NONE', #58016 ) ;
#15525=PLANE ( 'NONE',  #58900 ) ;
#15526=CARTESIAN_POINT ( 'NONE',  ( -80.44898789460346222, -25.29552500624826195, 4.507972869655594295 ) ) ;
#15528=AXIS2_PLACEMENT_3D ( 'NONE', #2645, #80763, #56938 ) ;
#15529=FACE_BOUND ( 'NONE', #89365, .T. ) ;
#15530=CARTESIAN_POINT ( 'NONE',  ( 18.72186718581493636, -5.619560887262019300, -1.500000000000002220 ) ) ;
#15532=CARTESIAN_POINT ( 'NONE',  ( 13.13055478438326773, -17.03443908202477886, 11.49999999999998934 ) ) ;
#15533=CARTESIAN_POINT ( 'NONE',  ( -128.6241754002568882, -23.73766607897672287, -1.055555164236423149 ) ) ;
#15537=CARTESIAN_POINT ( 'NONE',  ( 20.53691900564983186, 10.01969956684014207, -1.500000000000002220 ) ) ;
#15539=ADVANCED_FACE ( 'NONE', ( #79823 ), #24730, .T. ) ;
#15540=B_SPLINE_CURVE_WITH_KNOTS ( 'NONE', 3,
 ( #14923, #68731, #85948, #61631, #46386, #62123, #93045, #24037, #69731, #55010, #62623, #93542, #209, #99650 ),
 .UNSPECIFIED., .F., .F.,
 ( 4, 2, 2, 2, 2, 2, 4 ),
 ( 1.734723475976807094E-18, 0.0001855958525969266134, 0.0003711917051938514920, 0.0007423834103877197891, 0.001113575115581588032, 0.001299170968178541994, 0.001484766820775495957 ),
 .UNSPECIFIED. ) ;
#15542=CARTESIAN_POINT ( 'NONE',  ( -96.60008899554439665, -23.48786465467241058, 11.44779295918254469 ) ) ;
#15543=CARTESIAN_POINT ( 'NONE',  ( -70.93828905505007754, -25.30664601920957324, 5.476242254610935944 ) ) ;
#15544=CARTESIAN_POINT ( 'NONE',  ( 5.980626343040887249, -19.09133569553460319, 11.49999999999999645 ) ) ;
#15545=CARTESIAN_POINT ( 'NONE',  ( -78.99596516450635875, -25.31594537816884127, 5.526333899285822859 ) ) ;
#15549=EDGE_LOOP ( 'NONE', ( #33760, #5404, #46240, #1520 ) ) ;
#15551=CARTESIAN_POINT ( 'NONE',  ( -92.62287095715005592, -23.48783264082479150, -1.443836473390063713 ) ) ;
#15552=EDGE_CURVE ( 'NONE', #97111, #1645, #27129, .T. ) ;
#15553=CARTESIAN_POINT ( 'NONE',  ( -18.42844947050907578, 11.51566461966115540, 11.49999999999998934 ) ) ;
#15554=CARTESIAN_POINT ( 'NONE',  ( -56.62287095715005592, -23.48786465467241413, 11.44779295918254824 ) ) ;
#15555=CARTESIAN_POINT ( 'NONE',  ( -13.18904525526904692, 14.46673508071025971, -1.500000000000002220 ) ) ;
#15556=CARTESIAN_POINT ( 'NONE',  ( -85.52287095715006160, -24.92604778743017491, 8.074972756849357225 ) ) ;
#15557=EDGE_CURVE ( 'NONE', #72155, #65722, #88955, .T. ) ;
#15558=EDGE_CURVE ( 'NONE', #56230, #82393, #25037, .T. ) ;
#15559=CARTESIAN_POINT ( 'NONE',  ( -41.46611000704998418, -25.27828342519987359, 4.188173683033348915 ) ) ;
#15561=CARTESIAN_POINT ( 'NONE',  ( -38.58953762381672448, -23.47596703998600276, 11.44779298504227505 ) ) ;
#15562=LINE ( 'NONE', #91190, #8606 ) ;
#15563=CARTESIAN_POINT ( 'NONE',  ( -1.452656003914881477, -20.50939586048694352, 11.49999999999999645 ) ) ;
#15566=ADVANCED_FACE ( 'NONE', ( #80331 ), #72732, .F. ) ;
#15567=ORIENTED_EDGE ( 'NONE', *, *, #11464, .T. ) ;
#15568=CARTESIAN_POINT ( 'NONE',  ( -100.5167721066480908, -25.31296450146793120, 4.733455254540654522 ) ) ;
#15570=CARTESIAN_POINT ( 'NONE',  ( -125.5200004750861638, -24.63419186844610920, 9.035850630976920428 ) ) ;
#15571=CARTESIAN_POINT ( 'NONE',  ( -85.62287095715004170, -24.52232992886362695, 0.6492154411906178035 ) ) ;
#15572=CARTESIAN_POINT ( 'NONE',  ( -25.53215482860445107, -24.93062936653361206, 5.039154709304365376 ) ) ;
#15573=CARTESIAN_POINT ( 'NONE',  ( -68.62287095715005592, -23.48783264082478439, -1.443836473390067265 ) ) ;
#15574=VECTOR ( 'NONE', #43530, 1000.000000000000114 ) ;
#15575=CARTESIAN_POINT ( 'NONE',  ( 11.75533340255842596, 19.88161105567325038, 11.49999999999999645 ) ) ;
#15576=CARTESIAN_POINT ( 'NONE',  ( -12.44792101662413408, -19.12764231104124946, 11.49999999999998934 ) ) ;
#15577=CARTESIAN_POINT ( 'NONE',  ( -74.55900427510123052, -23.73766607897670511, -1.055555164236458898 ) ) ;
#15578=CARTESIAN_POINT ( 'NONE',  ( -88.52287095715001897, -23.73907113216989373, -1.053371485793251017 ) ) ;
#15579=CARTESIAN_POINT ( 'NONE',  ( -59.27315846036497504, -25.26302882147717099, 3.719515914026431336 ) ) ;
#15580=CARTESIAN_POINT ( 'NONE',  ( 14.18375884139645215, 17.39688726336347102, 11.49999999999999645 ) ) ;
#15583=CARTESIAN_POINT ( 'NONE',  ( -43.52287095715007581, -23.95044443724991723, 10.65354141964649415 ) ) ;
#15584=CARTESIAN_POINT ( 'NONE',  ( 18.54397492014093984, 11.73900455106235086, 11.49999999999998934 ) ) ;
#15587=CARTESIAN_POINT ( 'NONE',  ( -87.58839707165199684, -24.35071581493543391, 9.817618358456025263 ) ) ;
#15588=PLANE ( 'NONE',  #1699 ) ;
#15589=CARTESIAN_POINT ( 'NONE',  ( -78.51706572721168698, -23.73766607897670511, -1.055555164236459342 ) ) ;
#15590=CARTESIAN_POINT ( 'NONE',  ( -97.22287095715006444, -23.47593901973090169, -1.443836447538996870 ) ) ;
#15593=CARTESIAN_POINT ( 'NONE',  ( 8.813945691637787405, 18.49579627399651471, 11.49999999999998934 ) ) ;
#15597=ORIENTED_EDGE ( 'NONE', *, *, #21732, .F. ) ;
#15599=CARTESIAN_POINT ( 'NONE',  ( 18.43541038833219758, -13.85303862407246811, 11.49999999999998934 ) ) ;
#15600=CARTESIAN_POINT ( 'NONE',  ( -72.62287095715005592, -29.50248528299804818, 1.056150453629036701 ) ) ;
#15601=CARTESIAN_POINT ( 'NONE',  ( 9.670762957215185196, 17.83519281925787325, -1.500000000000002220 ) ) ;
#15602=AXIS2_PLACEMENT_3D ( 'NONE', #3212, #88433, #34153 ) ;
#15603=VERTEX_POINT ( 'NONE', #20914 ) ;
#15604=CARTESIAN_POINT ( 'NONE',  ( -48.52287095715006160, -24.50321055353804667, 9.387540953477520489 ) ) ;
#15605=CARTESIAN_POINT ( 'NONE',  ( -72.52287095715007581, -24.64898659630367916, 1.056161002820824368 ) ) ;
#15606=VECTOR ( 'NONE', #38289, 1000.000000000000114 ) ;
#15607=FACE_OUTER_BOUND ( 'NONE', #91420, .T. ) ;
#15608=CARTESIAN_POINT ( 'NONE',  ( -70.53858138727555627, -24.73486907724917572, 1.287355809206963908 ) ) ;
#15609=CARTESIAN_POINT ( 'NONE',  ( 19.19993882694861753, 9.668096177433461946, 11.49999999999999645 ) ) ;
#15611=CARTESIAN_POINT ( 'NONE',  ( -75.62528691939071734, -24.92564183028979130, 1.928384488918256645 ) ) ;
#15612=CARTESIAN_POINT ( 'NONE',  ( -61.63716569185557148, -24.15620529776628089, 10.23563542870660825 ) ) ;
#15614=CARTESIAN_POINT ( 'NONE',  ( 19.40724743217988291, -7.346346906864608783, 11.49999999999998934 ) ) ;
#15616=CARTESIAN_POINT ( 'NONE',  ( -32.62287095715004881, -29.50248528299804818, 1.056150453629029817 ) ) ;
#15618=EDGE_CURVE ( 'NONE', #91541, #96024, #36834, .T. ) ;
#15620=CARTESIAN_POINT ( 'NONE',  ( -48.52287095715004739, -23.96127896942158486, -0.6493128930934110032 ) ) ;
#15622=ORIENTED_EDGE ( 'NONE', *, *, #44619, .T. ) ;
#15623=ADVANCED_FACE ( 'NONE', ( #35665 ), #37149, .F. ) ;
#15626=CARTESIAN_POINT ( 'NONE',  ( -65.64505387063937292, -24.15503026093916006, -0.2815557561904380446 ) ) ;
#15627=CARTESIAN_POINT ( 'NONE',  ( 14.26656746985186608, 16.74056184347216458, 11.49999999999999645 ) ) ;
#15628=EDGE_CURVE ( 'NONE', #64178, #33243, #82820, .T. ) ;
#15629=CARTESIAN_POINT ( 'NONE',  ( -89.55151923034836159, -24.15620529776628445, 10.23563542870660115 ) ) ;
#15630=CARTESIAN_POINT ( 'NONE',  ( 15.50834587592193259, -16.38432980155966590, -1.500000000000002220 ) ) ;
#15631=B_SPLINE_CURVE_WITH_KNOTS ( 'NONE', 3,
 ( #79346, #86463, #47912, #9839 ),
 .UNSPECIFIED., .F., .F.,
 ( 4, 4 ),
 ( 2.775557561562891351E-17, 9.999999999994735322E-05 ),
 .UNSPECIFIED. ) ;
#15634=CARTESIAN_POINT ( 'NONE',  ( 11.23609023086081038, -17.74952302366565604, -1.500000000000002220 ) ) ;
#15636=DIRECTION ( 'NONE',  ( -3.773278334453079030E-23, 0.9999999999976377785, 2.173523156925979128E-06 ) ) ;
#15637=ORIENTED_EDGE ( 'NONE', *, *, #72612, .F. ) ;
#15640=CARTESIAN_POINT ( 'NONE',  ( -66.49289369796184701, -24.65952944569304250, 1.056160979905692798 ) ) ;
#15641=CARTESIAN_POINT ( 'NONE',  ( -21.28347836979250118, 3.227085873532868021, -1.500000000000002220 ) ) ;
#15642=CARTESIAN_POINT ( 'NONE',  ( -100.5228709571500616, -23.47596703998600631, 11.44779298504228215 ) ) ;
#15643=ORIENTED_EDGE ( 'NONE', *, *, #83583, .T. ) ;
#15644=CARTESIAN_POINT ( 'NONE',  ( -0.2625952501129409367, 21.13516572482953748, 11.49999999999998934 ) ) ;
#15646=CARTESIAN_POINT ( 'NONE',  ( -51.44452858623887437, -25.26041045480337388, 7.233629632149025213 ) ) ;
#15647=CARTESIAN_POINT ( 'NONE',  ( -121.6240037161720409, -24.51314013834316441, 0.6176544820404217262 ) ) ;
#15648=CARTESIAN_POINT ( 'NONE',  ( -79.62287095715005592, -24.64898659630528854, 1.056161002820826145 ) ) ;
#15649=CARTESIAN_POINT ( 'NONE',  ( -80.92287095715010992, -23.47593901973090524, -1.443836447538997536 ) ) ;
#15650=CARTESIAN_POINT ( 'NONE',  ( -21.91774099701738621, 3.392077650570975766, -1.500000000000002220 ) ) ;
#15652=EDGE_CURVE ( 'NONE', #79759, #25743, #519, .T. ) ;
#15655=CARTESIAN_POINT ( 'NONE',  ( -37.57003923573987691, -23.48783264082477729, -1.443836473390075703 ) ) ;
#15656=CARTESIAN_POINT ( 'NONE',  ( -126.5562100404590211, -23.73766607897670511, -1.055555164236450238 ) ) ;
#15660=ADVANCED_FACE ( 'NONE', ( #82817 ), #64502, .T. ) ;
#15661=CARTESIAN_POINT ( 'NONE',  ( 18.36381783059253081, 6.383776564742674964, -1.500000000000002220 ) ) ;
#15662=CARTESIAN_POINT ( 'NONE',  ( -6.079122355442096115, 20.50309271558274915, 11.49999999999998934 ) ) ;
#15663=CARTESIAN_POINT ( 'NONE',  ( -64.52287095715006160, -24.65952944569304606, 1.056160979905695463 ) ) ;
#15665=CARTESIAN_POINT ( 'NONE',  ( -123.5228709571500616, -24.64898659630368627, 1.056161002820833028 ) ) ;
#15666=CARTESIAN_POINT ( 'NONE',  ( -101.1965263674405691, -25.27360055340518841, 3.665446404013341208 ) ) ;
#15667=CARTESIAN_POINT ( 'NONE',  ( 12.08046422559826816, 19.21373320108137861, -1.500000000000002220 ) ) ;
#15669=VECTOR ( 'NONE', #81231, 1000.000000000000114 ) ;
#15672=CARTESIAN_POINT ( 'NONE',  ( -127.6228709571500559, -23.96127896941633750, -0.6493128931037727147 ) ) ;
#15673=CARTESIAN_POINT ( 'NONE',  ( 4.300141163375406528, 19.41444791797076874, 11.49999999999999645 ) ) ;
#15674=CARTESIAN_POINT ( 'NONE',  ( -123.5905687669561530, -23.96169478059714919, 10.65365249895717348 ) ) ;
#15676=CARTESIAN_POINT ( 'NONE',  ( -60.25625423781919920, -25.20074414427590170, 3.409327697718777195 ) ) ;
#15678=CARTESIAN_POINT ( 'NONE',  ( -40.62287095715005592, -23.84081130438200091, 10.88220057463248658 ) ) ;
#15681=CARTESIAN_POINT ( 'NONE',  ( 20.17453868081960167, 7.849935799312063089, -1.500000000000002220 ) ) ;
#15683=CARTESIAN_POINT ( 'NONE',  ( -8.724563080612403709, -17.33930400145671413, -1.500000000000002220 ) ) ;
#15685=CARTESIAN_POINT ( 'NONE',  ( -55.54036855594094391, -24.52399227489126687, 9.353111116836526406 ) ) ;
#15686=EDGE_CURVE ( 'NONE', #52813, #6577, #69607, .T. ) ;
#15687=CARTESIAN_POINT ( 'NONE',  ( 16.46483878678964174, 11.07114234313464252, 11.49999999999998934 ) ) ;
#15689=CARTESIAN_POINT ( 'NONE',  ( -6.898722100468609675, -19.10483383855023476, 11.49999999999999645 ) ) ;
#15690=CARTESIAN_POINT ( 'NONE',  ( -80.51503367831445246, -23.85016227208580730, -0.8807180028928341953 ) ) ;
#15692=DIRECTION ( 'NONE',  ( -3.773278334444167608E-23, 1.000000000000000000, 0.000000000000000000 ) ) ;
#15695=FACE_OUTER_BOUND ( 'NONE', #92354, .T. ) ;
#15696=CARTESIAN_POINT ( 'NONE',  ( -49.08163135806235289, -25.31601931085639023, 5.465038190089022585 ) ) ;
#15697=CARTESIAN_POINT ( 'NONE',  ( -40.57354567782093824, -23.48786465467240347, 11.44779295918255180 ) ) ;
#15699=CARTESIAN_POINT ( 'NONE',  ( 18.81927703376926786, -7.057843677351100631, -1.500000000000002220 ) ) ;
#15703=CARTESIAN_POINT ( 'NONE',  ( -91.62287095715007013, -24.35013146730204525, 9.818937971375104823 ) ) ;
#15705=CARTESIAN_POINT ( 'NONE',  ( -16.32851894532483783, 16.03542138455653898, 11.49999999999999645 ) ) ;
#15706=CARTESIAN_POINT ( 'NONE',  ( 1.118074629359579797, -22.68859683979520980, 11.49999999999998934 ) ) ;
#15709=CARTESIAN_POINT ( 'NONE',  ( -126.5228709571500616, -24.66019654487200441, 8.947790411086108620 ) ) ;
#15713=CARTESIAN_POINT ( 'NONE',  ( -111.5228709571500616, -23.47596703998600631, 11.44779298504228038 ) ) ;
#15714=ORIENTED_EDGE ( 'NONE', *, *, #33430, .T. ) ;
#15715=CARTESIAN_POINT ( 'NONE',  ( 17.64890103348723116, 10.21726211432410203, -1.500000000000002220 ) ) ;
#15716=ORIENTED_EDGE ( 'NONE', *, *, #100039, .T. ) ;
#15717=CARTESIAN_POINT ( 'NONE',  ( -22.04953120734539240, -6.464106996104416858, -1.500000000000002220 ) ) ;
#15718=CARTESIAN_POINT ( 'NONE',  ( -54.61289481623843756, -23.48786465467240347, 11.44779295918255357 ) ) ;
#15719=ORIENTED_EDGE ( 'NONE', *, *, #61370, .T. ) ;
#15720=CARTESIAN_POINT ( 'NONE',  ( -101.4686356869278967, -25.21739261586568048, 6.465307737249717412 ) ) ;
#15721=VECTOR ( 'NONE', #80677, 1000.000000000000114 ) ;
#15722=CARTESIAN_POINT ( 'NONE',  ( -81.48149462243461016, -25.24685308744633261, 6.293942982122115559 ) ) ;
#15723=B_SPLINE_CURVE_WITH_KNOTS ( 'NONE', 3,
 ( #50011, #3343, #72343, #79435 ),
 .UNSPECIFIED., .F., .F.,
 ( 4, 4 ),
 ( 0.000000000000000000, 9.999999999998206125E-05 ),
 .UNSPECIFIED. ) ;
#15725=CARTESIAN_POINT ( 'NONE',  ( 9.714863677370791706, 19.00186346016302608, 11.49999999999999645 ) ) ;
#15726=ORIENTED_EDGE ( 'NONE', *, *, #93007, .F. ) ;
#15727=ORIENTED_EDGE ( 'NONE', *, *, #15745, .T. ) ;
#15728=CARTESIAN_POINT ( 'NONE',  ( 7.537409830304743430, 20.87355781386819942, -1.500000000000002220 ) ) ;
#15729=CARTESIAN_POINT ( 'NONE',  ( 13.18972694569024640, 15.87703813876158598, 11.49999999999998934 ) ) ;
#15734=CARTESIAN_POINT ( 'NONE',  ( -71.72373620137601336, -25.31392322340849432, 5.203679841770401104 ) ) ;
#15735=ORIENTED_EDGE ( 'NONE', *, *, #96169, .F. ) ;
#15738=CARTESIAN_POINT ( 'NONE',  ( -91.50906031749687486, -24.34968618360934300, 0.1864209137778843617 ) ) ;
#15739=AXIS2_PLACEMENT_3D ( 'NONE', #31880, #27647, #79547 ) ;
#15741=CARTESIAN_POINT ( 'NONE',  ( -58.55359039973971846, -23.96169478059713143, 10.65365249895718058 ) ) ;
#15742=DIRECTION ( 'NONE',  ( -3.773278334444166432E-23, 1.000000000000000000, 0.000000000000000000 ) ) ;
#15743=CARTESIAN_POINT ( 'NONE',  ( 19.93353245626563819, -6.116835970281883306, -1.500000000000002220 ) ) ;
#15744=CARTESIAN_POINT ( 'NONE',  ( -21.05831370385527990, 5.553659732266172711, 11.49999999999999645 ) ) ;
#15745=EDGE_CURVE ( 'NONE', #79100, #19988, #85314, .T. ) ;
#15746=CARTESIAN_POINT ( 'NONE',  ( -98.52287095715006160, -29.50248528299804818, 1.056150453629042030 ) ) ;
#15748=CARTESIAN_POINT ( 'NONE',  ( -6.716530693746936898, -21.44081863256500142, 11.49999999999998934 ) ) ;
#15750=CARTESIAN_POINT ( 'NONE',  ( -118.5167408753442260, -24.66019654487199730, 8.947790411086115725 ) ) ;
#15751=PLANE ( 'NONE',  #25867 ) ;
#15754=EDGE_CURVE ( 'NONE', #47315, #48546, #39647, .T. ) ;
#15755=ORIENTED_EDGE ( 'NONE', *, *, #26300, .T. ) ;
#15756=ORIENTED_EDGE ( 'NONE', *, *, #47622, .T. ) ;
#15757=CARTESIAN_POINT ( 'NONE',  ( 20.50650179695670872, -5.950058665555418180, -1.500000000000002220 ) ) ;
#15759=CARTESIAN_POINT ( 'NONE',  ( -4.359323203648655998, -20.60729432550360585, 11.49999999999998934 ) ) ;
#15760=CARTESIAN_POINT ( 'NONE',  ( -30.49166226875084718, -24.48011564457811673, 0.5642940035406436294 ) ) ;
#15762=B_SPLINE_CURVE_WITH_KNOTS ( 'NONE', 3,
 ( #100295, #77471, #93202, #60284, #85093, #84596 ),
 .UNSPECIFIED., .F., .F.,
 ( 4, 2, 4 ),
 ( 6.384118678612693437E-06, 0.001386860460828375202, 0.002767336802978137989 ),
 .UNSPECIFIED. ) ;
#15764=CARTESIAN_POINT ( 'NONE',  ( -9.458160343781703006, 19.84743614482962926, -1.500000000000002220 ) ) ;
#15765=CARTESIAN_POINT ( 'NONE',  ( -87.52287095715006160, -23.47593901973090524, -1.443836447538996648 ) ) ;
#15767=DIRECTION ( 'NONE',  ( 3.773278334444167608E-23, -1.000000000000000000, 0.000000000000000000 ) ) ;
#15769=CARTESIAN_POINT ( 'NONE',  ( -18.00717387566553995, 10.56535500573724740, 11.49999999999999645 ) ) ;
#15772=CARTESIAN_POINT ( 'NONE',  ( -128.9228709571500531, -23.47596703998600631, 11.44779298504227860 ) ) ;
#15774=CARTESIAN_POINT ( 'NONE',  ( -20.38992447862095148, -24.51869592734078651, 6.147794833475635379 ) ) ;
#15775=CARTESIAN_POINT ( 'NONE',  ( 0.1273799443098547757, 21.28700333820561497, 11.49999999999998934 ) ) ;
#15777=CARTESIAN_POINT ( 'NONE',  ( -107.5552259268662993, -23.96169478059713853, 10.65365249895717348 ) ) ;
#15778=CARTESIAN_POINT ( 'NONE',  ( -35.52287095715006870, -29.50247984919015209, -1.443849546365060466 ) ) ;
#15780=CARTESIAN_POINT ( 'NONE',  ( 12.95044643391442030, 18.39415735498938176, -1.500000000000002220 ) ) ;
#15781=B_SPLINE_SURFACE_WITH_KNOTS ( 'NONE', 3, 3, ( 
 ( #35108, #27495, #58452, #72670 ),
 ( #34108, #89384, #12743, #84639 ),
 ( #15626, #5145, #67066, #76513 ),
 ( #30857, #45593, #30352, #46593 ),
 ( #407, #69921, #77518, #43714 ),
 ( #66580, #89883, #74649, #38471 ),
 ( #20352, #23738, #100341, #35608 ),
 ( #7516, #97492, #20857, #68918 ),
 ( #85139, #37968, #92250, #8018 ),
 ( #61326, #77015, #99844, #69423 ) ),
 .UNSPECIFIED., .F., .F., .F.,
 ( 4, 3, 3, 4 ),
 ( 4, 4 ),
 ( 0.0004766839783815427639, 0.1491231665100170578, 0.2234464077758348266, 0.2977696490416525954 ),
 ( 0.6495724517647905039, 0.6509722533490930330 ),
 .UNSPECIFIED. ) ;
#15783=ORIENTED_EDGE ( 'NONE', *, *, #15797, .F. ) ;
#15785=CARTESIAN_POINT ( 'NONE',  ( -18.24527198174902765, 7.358211898524878336, 11.49999999999999645 ) ) ;
#15786=CARTESIAN_POINT ( 'NONE',  ( -28.62287095715004526, -24.19530606561500008, 0.1850819291420055523 ) ) ;
#15789=CARTESIAN_POINT ( 'NONE',  ( -99.63195852548790299, -23.96119346886881374, -0.6495511937831867089 ) ) ;
#15790=CARTESIAN_POINT ( 'NONE',  ( -36.52287095715007581, -23.95044443724991723, 10.65354141964649415 ) ) ;
#15791=CARTESIAN_POINT ( 'NONE',  ( -100.1102081092206930, -25.31439547524505684, 5.264240186624079776 ) ) ;
#15792=VECTOR ( 'NONE', #29897, 1000.000000000000114 ) ;
#15794=CARTESIAN_POINT ( 'NONE',  ( 5.037983044326730386, -19.10262670698400100, 11.49999999999998934 ) ) ;
#15797=EDGE_CURVE ( 'NONE', #16286, #85354, #31974, .T. ) ;
#15800=ADVANCED_FACE ( 'NONE', ( #1095 ), #81537, .T. ) ;
#15801=VERTEX_POINT ( 'NONE', #9706 ) ;
#15802=PLANE ( 'NONE',  #15930 ) ;
#15803=CARTESIAN_POINT ( 'NONE',  ( -53.62287095715003460, -24.33832256526968507, 0.1851278514119814866 ) ) ;
#15804=CARTESIAN_POINT ( 'NONE',  ( -81.48149462243459595, -25.23679622552714363, 6.293943003980942308 ) ) ;
#15805=CARTESIAN_POINT ( 'NONE',  ( -98.89994392110364174, -25.26638266936259214, 6.299691109395265443 ) ) ;
#15807=VECTOR ( 'NONE', #98506, 1000.000000000000114 ) ;
#15808=CARTESIAN_POINT ( 'NONE',  ( -67.52287095715006160, -24.64965694238407323, 8.947790433994200043 ) ) ;
#15809=PLANE ( 'NONE',  #51079 ) ;
#15810=CARTESIAN_POINT ( 'NONE',  ( -13.93161493328335432, -14.37010051631055418, 11.49999999999998934 ) ) ;
#15812=CARTESIAN_POINT ( 'NONE',  ( -45.49172329232699497, -24.40133493613049964, 9.663955038902802386 ) ) ;
#15814=B_SPLINE_CURVE_WITH_KNOTS ( 'NONE', 3,
 ( #16951, #42320, #80351, #78832, #9333, #40296 ),
 .UNSPECIFIED., .F., .F.,
 ( 4, 2, 4 ),
 ( 6.384118696476699610E-06, 0.001386860460837304257, 0.002767336802978131918 ),
 .UNSPECIFIED. ) ;
#15816=CARTESIAN_POINT ( 'NONE',  ( -109.4273347235498193, -25.18430276407331903, 3.857971852524231249 ) ) ;
#15818=CARTESIAN_POINT ( 'NONE',  ( -100.5228709571500616, -23.48786465467242479, 11.44779295918254114 ) ) ;
#15823=ORIENTED_EDGE ( 'NONE', *, *, #15652, .T. ) ;
#15824=CARTESIAN_POINT ( 'NONE',  ( 17.44645523915803764, -10.38078700900905993, 11.49999999999998934 ) ) ;
#15826=AXIS2_PLACEMENT_3D ( 'NONE', #47109, #1432, #55230 ) ;
#15827=CARTESIAN_POINT ( 'NONE',  ( -76.62287095715007013, -23.48783264082478084, -1.443836473390065489 ) ) ;
#15828=ORIENTED_EDGE ( 'NONE', *, *, #27558, .T. ) ;
#15830=FACE_OUTER_BOUND ( 'NONE', #60017, .T. ) ;
#15831=CARTESIAN_POINT ( 'NONE',  ( 18.81927703376926786, -7.057843677351100631, -1.500000000000002220 ) ) ;
#15832=CARTESIAN_POINT ( 'NONE',  ( -6.733481718715807141, 19.98004043397084928, 11.49999999999999645 ) ) ;
#15833=CARTESIAN_POINT ( 'NONE',  ( -4.051365815588555463, -21.74199345402511696, -1.500000000000002220 ) ) ;
#15834=CARTESIAN_POINT ( 'NONE',  ( 4.502618398017903090, 20.03723546437915104, -1.500000000000002220 ) ) ;
#15835=CARTESIAN_POINT ( 'NONE',  ( -60.49079332354545357, -24.63355581998385446, 0.9682620441943891043 ) ) ;
#15838=ORIENTED_EDGE ( 'NONE', *, *, #71117, .T. ) ;
#15840=CARTESIAN_POINT ( 'NONE',  ( -70.52287095715007581, -24.99156044556120548, 7.747789690856173195 ) ) ;
#15841=ORIENTED_EDGE ( 'NONE', *, *, #83710, .T. ) ;
#15842=B_SPLINE_CURVE_WITH_KNOTS ( 'NONE', 3,
 ( #81478, #18563, #41414, #18068, #49538, #3370 ),
 .UNSPECIFIED., .F., .F.,
 ( 4, 2, 4 ),
 ( 0.000000000000000000, 0.001380901958385387894, 0.002761803916770775788 ),
 .UNSPECIFIED. ) ;
#15844=ORIENTED_EDGE ( 'NONE', *, *, #38567, .F. ) ;
#15846=DIRECTION ( 'NONE',  ( 1.000000000000000000, 3.773278334444167608E-23, 8.201307833595939069E-29 ) ) ;
#15847=DIRECTION ( 'NONE',  ( -3.773278334453079618E-23, 0.9999999999976377785, 2.173523156925979975E-06 ) ) ;
#15848=FACE_OUTER_BOUND ( 'NONE', #38576, .T. ) ;
#15849=CARTESIAN_POINT ( 'NONE',  ( -18.12278953325389708, -9.833843834435361586, -1.500000000000002220 ) ) ;
#15850=CARTESIAN_POINT ( 'NONE',  ( 11.83326311654409935, 18.06170320929925310, 11.49999999999999645 ) ) ;
#15853=CARTESIAN_POINT ( 'NONE',  ( -42.22287095715005734, -23.47596703998600276, 11.44779298504227860 ) ) ;
#15855=CARTESIAN_POINT ( 'NONE',  ( 3.152853332073482839, 22.16862046936333286, -1.500000000000002220 ) ) ;
#15856=AXIS2_PLACEMENT_3D ( 'NONE', #37892, #84059, #77432 ) ;
#15858=CARTESIAN_POINT ( 'NONE',  ( -103.6228709571500559, -29.50248528299804818, 1.056150453629042030 ) ) ;
#15861=CARTESIAN_POINT ( 'NONE',  ( -100.4293229868110160, -25.31235227439576363, 4.721894440410697058 ) ) ;
#15862=CARTESIAN_POINT ( 'NONE',  ( -35.52193564919225111, -23.48786465467240347, 11.44779295918255180 ) ) ;
#15863=EDGE_CURVE ( 'NONE', #11023, #29369, #50138, .T. ) ;
#15864=CARTESIAN_POINT ( 'NONE',  ( -13.90609606471210391, -15.62508359690603221, -1.500000000000002220 ) ) ;
#15865=EDGE_CURVE ( 'NONE', #59928, #18750, #8966, .T. ) ;
#15866=EDGE_LOOP ( 'NONE', ( #9512, #80742, #76305, #90470 ) ) ;
#15870=ORIENTED_EDGE ( 'NONE', *, *, #94562, .F. ) ;
#15871=CARTESIAN_POINT ( 'NONE',  ( -101.9507253916653440, -29.50249654204571215, 6.236241424690079249 ) ) ;
#15872=CARTESIAN_POINT ( 'NONE',  ( -20.37118330240554087, -5.769015352940915164, -1.500000000000002220 ) ) ;
#15873=EDGE_LOOP ( 'NONE', ( #35647, #32233, #16205, #64146 ) ) ;
#15875=CARTESIAN_POINT ( 'NONE',  ( 10.97640485992876691, 18.82695874702771377, 11.49999999999998934 ) ) ;
#15876=CARTESIAN_POINT ( 'NONE',  ( -60.55620429048339304, -23.47596703998600276, 11.44779298504227505 ) ) ;
#15878=LINE ( 'NONE', #29607, #82590 ) ;
#15879=DIRECTION ( 'NONE',  ( -3.773278334453080206E-23, 0.9999999999976377785, 2.173523156925979975E-06 ) ) ;
#15880=CARTESIAN_POINT ( 'NONE',  ( 4.919149715316761373, 21.27959583485438344, -1.500000000000002220 ) ) ;
#15888=B_SPLINE_CURVE_WITH_KNOTS ( 'NONE', 3,
 ( #13160, #45135, #74570, #97895 ),
 .UNSPECIFIED., .F., .F.,
 ( 4, 4 ),
 ( 3.422183298990500128E-11, 0.002177849098239042699 ),
 .UNSPECIFIED. ) ;
#15889=ORIENTED_EDGE ( 'NONE', *, *, #30809, .T. ) ;
#15890=DIRECTION ( 'NONE',  ( -1.000000000000000000, -3.773278334444167608E-23, -8.201307833595939069E-29 ) ) ;
#15892=CARTESIAN_POINT ( 'NONE',  ( 0.06830352742921809439, -21.21198074455918814, 11.49999999999998934 ) ) ;
#15893=CARTESIAN_POINT ( 'NONE',  ( -125.5228709571500616, -23.47593901973090524, -1.443836447538996204 ) ) ;
#15894=CARTESIAN_POINT ( 'NONE',  ( -80.40044610398997804, -25.03138299335276429, 7.562159499395756157 ) ) ;
#15895=DIRECTION ( 'NONE',  ( -3.773278334453079618E-23, 0.9999999999976377785, 2.173523156925979975E-06 ) ) ;
#15897=CARTESIAN_POINT ( 'NONE',  ( 18.67713048845720181, -5.233370074711279685, -1.500000000000002220 ) ) ;
#15898=CARTESIAN_POINT ( 'NONE',  ( -69.56540253034138743, -25.29932401351703675, 5.636500610589230575 ) ) ;
#15900=CARTESIAN_POINT ( 'NONE',  ( -0.2416374764669896869, -19.45557994585427508, 11.49999999999999645 ) ) ;
#15902=CARTESIAN_POINT ( 'NONE',  ( -80.11904448212310115, -25.13254330329641917, 7.046576512759410882 ) ) ;
#15905=CARTESIAN_POINT ( 'NONE',  ( -54.52287095715006870, -29.50250786944525672, 11.44777988621624054 ) ) ;
#15906=CARTESIAN_POINT ( 'NONE',  ( -64.62287095715005592, -24.50216790748205398, 0.6166512839542535040 ) ) ;
#15907=EDGE_CURVE ( 'NONE', #3681, #53534, #17312, .T. ) ;
#15908=CARTESIAN_POINT ( 'NONE',  ( -93.54470257384001286, -24.66019654487200441, 8.947790411086105067 ) ) ;
#15909=CARTESIAN_POINT ( 'NONE',  ( -15.16444148636751521, -12.51942901160708921, -1.500000000000002220 ) ) ;
#15911=PLANE ( 'NONE',  #57462 ) ;
#15913=CARTESIAN_POINT ( 'NONE',  ( 7.401388779597747103, 20.28278527911644247, -1.500000000000002220 ) ) ;
#15914=CARTESIAN_POINT ( 'NONE',  ( -40.52633905974123962, -24.83618233451449342, 1.606449574219539711 ) ) ;
#15916=CARTESIAN_POINT ( 'NONE',  ( -3.733506833432379768, 22.73668382284982314, -1.500000000000002220 ) ) ;
#15919=DIRECTION ( 'NONE',  ( 3.773278334444167608E-23, -1.000000000000000000, 0.000000000000000000 ) ) ;
#15921=CARTESIAN_POINT ( 'NONE',  ( -121.5924664832264881, -23.48786465467241413, 11.44779295918253581 ) ) ;
#15922=FACE_OUTER_BOUND ( 'NONE', #77731, .T. ) ;
#15923=CARTESIAN_POINT ( 'NONE',  ( -111.0058427071010527, -25.10921409436117813, 2.995661355163232731 ) ) ;
#15924=CARTESIAN_POINT ( 'NONE',  ( -129.5899315059631647, -23.73766607897671577, -1.055555164236443577 ) ) ;
#15925=B_SPLINE_CURVE_WITH_KNOTS ( 'NONE', 3,
 ( #124, #8744, #54921, #62533, #23954, #54418 ),
 .UNSPECIFIED., .F., .F.,
 ( 4, 2, 4 ),
 ( 0.000000000000000000, 0.001380764517854760412, 0.002761529035709520824 ),
 .UNSPECIFIED. ) ;
#15926=CARTESIAN_POINT ( 'NONE',  ( -99.19491584893809488, -25.31565985344014180, 4.406300475431831565 ) ) ;
#15927=CARTESIAN_POINT ( 'NONE',  ( 19.23997954701083657, -5.074110557352235595, -1.500000000000002220 ) ) ;
#15928=CARTESIAN_POINT ( 'NONE',  ( -101.3316698755723451, -25.26509388656816668, 3.891060496532311230 ) ) ;
#15929=CARTESIAN_POINT ( 'NONE',  ( -4.880483578727112359, 19.22116399702514045, -1.500000000000002220 ) ) ;
#15930=AXIS2_PLACEMENT_3D ( 'NONE', #8203, #88214, #26807 ) ;
#15932=CARTESIAN_POINT ( 'NONE',  ( -39.08546997848264226, -25.29116740964227361, 3.855771218128337896 ) ) ;
#15934=CARTESIAN_POINT ( 'NONE',  ( -5.109682455881146446, -20.12422286529520932, 11.49999999999999645 ) ) ;
#15937=FACE_OUTER_BOUND ( 'NONE', #32222, .T. ) ;
#15938=CARTESIAN_POINT ( 'NONE',  ( 9.298244000614250382, 20.81247324795305431, 11.49999999999999645 ) ) ;
#15939=EDGE_LOOP ( 'NONE', ( #35072, #7029, #37447, #10122 ) ) ;
#15940=CARTESIAN_POINT ( 'NONE',  ( -69.62709768445154168, -24.51314013834315375, 0.6176544820404143987 ) ) ;
#15941=CARTESIAN_POINT ( 'NONE',  ( -69.34467329208345632, -25.23938715212924322, 6.270976422656406868 ) ) ;
#15943=AXIS2_PLACEMENT_3D ( 'NONE', #1101, #40670, #48284 ) ;
#15944=CARTESIAN_POINT ( 'NONE',  ( -18.21026628907936029, 8.684577975296603469, 11.49999999999998934 ) ) ;
#15945=DIRECTION ( 'NONE',  ( 0.000000000000000000, 0.9999999999976377785, 2.173523156925979128E-06 ) ) ;
#15946=CARTESIAN_POINT ( 'NONE',  ( -40.91555040693666712, -25.30563909050597360, 4.985614010301523180 ) ) ;
#15947=ORIENTED_EDGE ( 'NONE', *, *, #28566, .T. ) ;
#15948=ORIENTED_EDGE ( 'NONE', *, *, #36144, .F. ) ;
#15949=FACE_OUTER_BOUND ( 'NONE', #85870, .T. ) ;
#15950=CARTESIAN_POINT ( 'NONE',  ( 16.68310095749102118, 15.68496000196893370, -1.500000000000002220 ) ) ;
#15951=CARTESIAN_POINT ( 'NONE',  ( -51.29535283968221648, -25.18439786647864409, 3.923498624102081056 ) ) ;
#15952=CARTESIAN_POINT ( 'NONE',  ( 19.28387207504633949, -9.851753786812027514, -1.500000000000002220 ) ) ;
#15954=CARTESIAN_POINT ( 'NONE',  ( -40.94688081444584782, -25.03284417894045788, 7.563176522466704910 ) ) ;
#15955=CARTESIAN_POINT ( 'NONE',  ( 18.69404101259207707, 9.334567778723176446, 11.49999999999999645 ) ) ;
#15956=VERTEX_POINT ( 'NONE', #33545 ) ;
#15957=CARTESIAN_POINT ( 'NONE',  ( -124.5216661205150928, -23.73766607897670866, -1.055555164236449350 ) ) ;
#15958=CARTESIAN_POINT ( 'NONE',  ( -7.807709442696729063, 20.60712426125841645, -1.500000000000002220 ) ) ;
#15960=CARTESIAN_POINT ( 'NONE',  ( -30.47287095715008576, -23.78634900524765072, 10.96467695203478065 ) ) ;
#15963=DIRECTION ( 'NONE',  ( 0.000000000000000000, 0.9999999999976377785, 2.173523156925979128E-06 ) ) ;
#15964=ORIENTED_EDGE ( 'NONE', *, *, #37313, .F. ) ;
#15965=CARTESIAN_POINT ( 'NONE',  ( -72.60740660736958318, -23.48786465467241058, 11.44779295918254824 ) ) ;
#15966=ORIENTED_EDGE ( 'NONE', *, *, #93289, .T. ) ;
#15967=ORIENTED_EDGE ( 'NONE', *, *, #18486, .T. ) ;
#15970=CARTESIAN_POINT ( 'NONE',  ( -95.62287095715007013, -24.92604778743017491, 8.074972756849353672 ) ) ;
#15971=CARTESIAN_POINT ( 'NONE',  ( -36.54575551158481517, -24.15543982623906771, -0.2315651400026672579 ) ) ;
#15972=CARTESIAN_POINT ( 'NONE',  ( 19.37909195245082472, -6.530858791768283211, -1.500000000000002220 ) ) ;
#15973=ORIENTED_EDGE ( 'NONE', *, *, #5208, .T. ) ;
#15974=CARTESIAN_POINT ( 'NONE',  ( -79.52287095715011844, -23.94994826722565406, -0.6494450866342715845 ) ) ;
#15976=CARTESIAN_POINT ( 'NONE',  ( -77.62287095715005592, -24.64898659630367916, 1.056161002820826145 ) ) ;
#15977=CARTESIAN_POINT ( 'NONE',  ( 9.404896790668452411, 20.21284700076377305, -1.500000000000002220 ) ) ;
#15978=CARTESIAN_POINT ( 'NONE',  ( -55.52287095715005449, -24.15516710230293285, 10.28746687063726384 ) ) ;
#15980=ORIENTED_EDGE ( 'NONE', *, *, #17363, .T. ) ;
#15981=CARTESIAN_POINT ( 'NONE',  ( -89.40841769935767047, -25.11033443737731474, 2.832404817301930056 ) ) ;
#15982=FACE_OUTER_BOUND ( 'NONE', #62919, .T. ) ;
#15983=EDGE_CURVE ( 'NONE', #60838, #75484, #53733, .T. ) ;
#15984=CARTESIAN_POINT ( 'NONE',  ( -20.33245250387252767, 4.503473919074798104, 11.49999999999998934 ) ) ;
#15987=CARTESIAN_POINT ( 'NONE',  ( -85.52287095715003318, -25.00182538069145011, 7.747789668545101094 ) ) ;
#15988=VERTEX_POINT ( 'NONE', #4606 ) ;
#15990=B_SPLINE_SURFACE_WITH_KNOTS ( 'NONE', 3, 3, ( 
 ( #91992, #60570, #53451, #14361 ),
 ( #29593, #44341, #91488, #31088 ),
 ( #83377, #84878, #77252, #21967 ),
 ( #84380, #144, #76747, #7757 ),
 ( #44837, #5763, #100078, #92487 ),
 ( #22463, #14861, #75269, #45827 ),
 ( #62058, #76260, #22957, #60070 ) ),
 .UNSPECIFIED., .F., .F., .F.,
 ( 4, 3, 4 ),
 ( 4, 4 ),
 ( 0.7945040050992251413, 0.8970133687736507877, 0.9995227324480764342 ),
 ( 0.8096997531712926133, 0.8110862888633306733 ),
 .UNSPECIFIED. ) ;
#15991=CARTESIAN_POINT ( 'NONE',  ( -111.6228709571500559, -29.50248528299804818, 1.056150453629043584 ) ) ;
#15992=CARTESIAN_POINT ( 'NONE',  ( 8.398332666215036824, -19.25654272332048578, -1.500000000000002220 ) ) ;
#15994=CARTESIAN_POINT ( 'NONE',  ( -86.62287095715005592, -24.66019654487199375, 8.947790411086124607 ) ) ;
#15996=CARTESIAN_POINT ( 'NONE',  ( -55.62287095715004170, -24.51254535404256174, 9.355368623467651190 ) ) ;
#15998=AXIS2_PLACEMENT_3D ( 'NONE', #89790, #20758, #13145 ) ;
#16000=CARTESIAN_POINT ( 'NONE',  ( -91.55620429048339304, -23.47593901973091235, -1.443836447539002865 ) ) ;
#16002=CARTESIAN_POINT ( 'NONE',  ( 9.120982285578694615, 20.23247719416018242, 11.49999999999999645 ) ) ;
#16004=EDGE_CURVE ( 'NONE', #43186, #20125, #81220, .T. ) ;
#16007=ORIENTED_EDGE ( 'NONE', *, *, #73379, .T. ) ;
#16008=CARTESIAN_POINT ( 'NONE',  ( 8.023449251107201974, -21.19570997880782670, -1.500000000000002220 ) ) ;
#16009=VECTOR ( 'NONE', #84507, 1000.000000000000114 ) ;
#16010=CARTESIAN_POINT ( 'NONE',  ( -29.05879606100779355, -25.09401859864639661, 6.517353683613309023 ) ) ;
#16011=ORIENTED_EDGE ( 'NONE', *, *, #76010, .F. ) ;
#16012=ORIENTED_EDGE ( 'NONE', *, *, #98497, .F. ) ;
#16015=CARTESIAN_POINT ( 'NONE',  ( 19.84801528777503776, 3.447069022702595742, 11.49999999999998934 ) ) ;
#16019=CARTESIAN_POINT ( 'NONE',  ( -15.79502933763849271, 15.79022959414610661, -1.500000000000002220 ) ) ;
#16022=ORIENTED_EDGE ( 'NONE', *, *, #72561, .T. ) ;
#16024=CARTESIAN_POINT ( 'NONE',  ( -94.63333269353616117, -23.96169478059713143, 10.65365249895717881 ) ) ;
#16025=CARTESIAN_POINT ( 'NONE',  ( -80.80255094563601403, -25.29787882119566333, 4.568986449336699174 ) ) ;
#16026=CARTESIAN_POINT ( 'NONE',  ( -68.52287095715006160, -23.96177878511308990, 10.65340807706330573 ) ) ;
#16028=EDGE_CURVE ( 'NONE', #84261, #60824, #51774, .T. ) ;
#16029=CARTESIAN_POINT ( 'NONE',  ( 3.395600993332231532, 19.23619202488179525, -1.500000000000002220 ) ) ;
#16030=CARTESIAN_POINT ( 'NONE',  ( -78.52287095715006160, -29.50250786944525672, 11.44777988621623521 ) ) ;
#16031=CARTESIAN_POINT ( 'NONE',  ( 0.6623178260406717976, 21.47796536025111536, -1.500000000000002220 ) ) ;
#16032=CARTESIAN_POINT ( 'NONE',  ( -128.5556220342893141, -24.34968618360935011, 0.1864209137779018477 ) ) ;
#16033=CARTESIAN_POINT ( 'NONE',  ( -54.62287095715005592, -24.64965695001467694, 8.947790433994185832 ) ) ;
#16034=CARTESIAN_POINT ( 'NONE',  ( -117.6228709571500559, -23.47593901973091235, -1.443836447538997536 ) ) ;
#16035=CARTESIAN_POINT ( 'NONE',  ( -111.6228709571500985, -23.73907113216991860, -1.053371485793221929 ) ) ;
#16036=CARTESIAN_POINT ( 'NONE',  ( 13.94817355369617751, 18.09530419158152625, -1.500000000000002220 ) ) ;
#16038=EDGE_CURVE ( 'NONE', #53278, #66705, #65984, .T. ) ;
#16040=CARTESIAN_POINT ( 'NONE',  ( -101.6228709571500559, -23.47593901973091235, -1.443836447539001089 ) ) ;
#16042=CARTESIAN_POINT ( 'NONE',  ( -13.81204400269958654, 14.50282280199826701, 11.49999999999999645 ) ) ;
#16043=CARTESIAN_POINT ( 'NONE',  ( -78.94416233434603214, -25.31594624443190611, 5.924886392682762626 ) ) ;
#16046=DIRECTION ( 'NONE',  ( -3.773278334453079030E-23, 0.9999999999976377785, 2.173523156925979128E-06 ) ) ;
#16047=ORIENTED_EDGE ( 'NONE', *, *, #39135, .T. ) ;
#16048=CARTESIAN_POINT ( 'NONE',  ( -50.62287095715006302, -24.63345952396258198, 9.038047939301517175 ) ) ;
#16049=B_SPLINE_CURVE_WITH_KNOTS ( 'NONE', 3,
 ( #50386, #33656, #72223, #49897, #64636, #11316 ),
 .UNSPECIFIED., .F., .F.,
 ( 4, 2, 4 ),
 ( 6.384118678609748304E-06, 0.001386860460828374334, 0.002767336802978138856 ),
 .UNSPECIFIED. ) ;
#16050=CARTESIAN_POINT ( 'NONE',  ( -17.16505717403991227, -13.39166244882208012, -1.500000000000002220 ) ) ;
#16051=CARTESIAN_POINT ( 'NONE',  ( -56.62287095715004881, -24.51387760970724372, 9.387446482453427166 ) ) ;
#16052=CARTESIAN_POINT ( 'NONE',  ( -17.62174901100306101, -8.731699659924187173, -1.500000000000002220 ) ) ;
#16054=CARTESIAN_POINT ( 'NONE',  ( -41.05392197949270638, -25.20725972110717095, 3.457283663102085125 ) ) ;
#16056=CARTESIAN_POINT ( 'NONE',  ( -56.62287095715009144, -23.95044443724992433, 10.65354141964650125 ) ) ;
#16057=CARTESIAN_POINT ( 'NONE',  ( -44.52287095715006160, -24.64898659630367916, 1.056161002820819261 ) ) ;
#16058=CARTESIAN_POINT ( 'NONE',  ( -17.20787902393383462, -11.26661214947554157, 11.49999999999999645 ) ) ;
#16059=CARTESIAN_POINT ( 'NONE',  ( -39.04303308397305727, -25.29008967749855685, 4.215216926603018166 ) ) ;
#16060=CARTESIAN_POINT ( 'NONE',  ( -120.5901076504048177, -24.40034930558991633, 0.3402023900116107336 ) ) ;
#16062=CARTESIAN_POINT ( 'NONE',  ( -22.20892344277460850, -4.061126821146308963, 11.49999999999999645 ) ) ;
#16063=VERTEX_POINT ( 'NONE', #5087 ) ;
#16064=CARTESIAN_POINT ( 'NONE',  ( -100.2051565992114632, -25.26387441634614817, 4.680112826087972522 ) ) ;
#16065=DIRECTION ( 'NONE',  ( -3.773278334453079030E-23, 0.9999999999976377785, 2.173523156925979128E-06 ) ) ;
#16067=CARTESIAN_POINT ( 'NONE',  ( -125.5556643051668715, -24.15602025860897584, 10.28564288303534013 ) ) ;
#16073=EDGE_CURVE ( 'NONE', #37981, #44655, #1794, .T. ) ;
#16075=ORIENTED_EDGE ( 'NONE', *, *, #54619, .F. ) ;
#16076=CARTESIAN_POINT ( 'NONE',  ( 11.92049557817732364, -19.74369927386287671, 11.49999999999999645 ) ) ;
#16077=CARTESIAN_POINT ( 'NONE',  ( 16.42120958226126604, -15.83219868413775622, -1.500000000000002220 ) ) ;
#16080=CARTESIAN_POINT ( 'NONE',  ( -96.59677831669986858, -23.73766607897670511, -1.055555164236452681 ) ) ;
#16081=CARTESIAN_POINT ( 'NONE',  ( -63.62287095715004881, -23.47593901973091235, -1.443836447539007972 ) ) ;
#16082=CARTESIAN_POINT ( 'NONE',  ( 18.78116726530667080, 12.29669497462397842, 11.49999999999999645 ) ) ;
#16083=EDGE_LOOP ( 'NONE', ( #81095, #45697, #89704, #5491 ) ) ;
#16085=B_SPLINE_CURVE_WITH_KNOTS ( 'NONE', 3,
 ( #97482, #11741, #27974, #35096, #96984, #27484 ),
 .UNSPECIFIED., .F., .F.,
 ( 4, 2, 4 ),
 ( 6.391158118963033063E-06, 0.001387004593080786580, 0.002767618028042609802 ),
 .UNSPECIFIED. ) ;
#16086=DIRECTION ( 'NONE',  ( -3.773278334453080206E-23, 0.9999999999976377785, 2.173523156925979975E-06 ) ) ;
#16087=CARTESIAN_POINT ( 'NONE',  ( -43.52287095715006870, -24.50321055353803601, 9.387540953477522265 ) ) ;
#16088=CARTESIAN_POINT ( 'NONE',  ( 6.821863743248424150, 20.85434273413645911, -1.500000000000002220 ) ) ;
#16089=CARTESIAN_POINT ( 'NONE',  ( -28.62287095715004881, -29.50248298729119867, -6.412432996800796609E-05 ) ) ;
#16090=CARTESIAN_POINT ( 'NONE',  ( -34.61899282609274309, -23.48786465467240347, 11.44779295918255535 ) ) ;
#16091=CARTESIAN_POINT ( 'NONE',  ( -121.5228709571500616, -24.64965694238408034, 8.947790433994191162 ) ) ;
#16095=ORIENTED_EDGE ( 'NONE', *, *, #79229, .F. ) ;
#16096=CARTESIAN_POINT ( 'NONE',  ( 13.99439195134931069, 14.96789054323355828, -1.500000000000002220 ) ) ;
#16097=ORIENTED_EDGE ( 'NONE', *, *, #75313, .F. ) ;
#16099=ORIENTED_EDGE ( 'NONE', *, *, #47546, .F. ) ;
#16100=ORIENTED_EDGE ( 'NONE', *, *, #4320, .F. ) ;
#16102=CARTESIAN_POINT ( 'NONE',  ( 14.79121776280621425, -17.69394282334246427, -1.500000000000002220 ) ) ;
#16103=CARTESIAN_POINT ( 'NONE',  ( -49.75863811138101056, -25.14487534265549229, 2.970700725601126635 ) ) ;
#16104=CARTESIAN_POINT ( 'NONE',  ( -17.48930418531667996, -10.34094407820366612, -1.500000000000002220 ) ) ;
#16106=LINE ( 'NONE', #56197, #72056 ) ;
#16107=CARTESIAN_POINT ( 'NONE',  ( -92.55472887090941470, -23.96119346886881374, -0.6495511937831873750 ) ) ;
#16108=CARTESIAN_POINT ( 'NONE',  ( -47.58953762381671737, -23.48783264082478084, -1.443836473390070596 ) ) ;
#16110=CARTESIAN_POINT ( 'NONE',  ( -20.49900048275977227, -6.559984590058941301, 11.49999999999999645 ) ) ;
#16112=CARTESIAN_POINT ( 'NONE',  ( -75.49128703381974503, -24.92564183028979130, 1.928384488918256645 ) ) ;
#16113=CARTESIAN_POINT ( 'NONE',  ( -61.49058198215474391, -24.66019654487199375, 8.947790411086119278 ) ) ;
#16115=CARTESIAN_POINT ( 'NONE',  ( -14.15296684469643118, 15.14645709676483420, 11.49999999999998934 ) ) ;
#16116=EDGE_CURVE ( 'NONE', #52940, #58462, #89335, .T. ) ;
#16119=ORIENTED_EDGE ( 'NONE', *, *, #54590, .T. ) ;
#16120=EDGE_CURVE ( 'NONE', #65549, #68269, #31786, .T. ) ;
#16121=CARTESIAN_POINT ( 'NONE',  ( -41.62875083135785559, -24.51419770103157347, 9.386484678747180510 ) ) ;
#16124=EDGE_LOOP ( 'NONE', ( #93883, #67280, #80043, #25372 ) ) ;
#16125=CARTESIAN_POINT ( 'NONE',  ( -53.52287095715006870, -23.47596703998600631, 11.44779298504229104 ) ) ;
#16127=CARTESIAN_POINT ( 'NONE',  ( -35.22287095715007155, -23.47596703998600276, 11.44779298504227683 ) ) ;
#16128=CARTESIAN_POINT ( 'NONE',  ( -10.85839155550747392, 19.17434714687634667, 11.49999999999999645 ) ) ;
#16131=CARTESIAN_POINT ( 'NONE',  ( 22.10748686624256720, -4.471405416651531795, -1.500000000000002220 ) ) ;
#16132=CARTESIAN_POINT ( 'NONE',  ( 18.73254098450790295, -9.497730595714260815, -1.500000000000002220 ) ) ;
#16133=EDGE_CURVE ( 'NONE', #75014, #25230, #83898, .T. ) ;
#16135=ORIENTED_EDGE ( 'NONE', *, *, #49541, .T. ) ;
#16137=EDGE_LOOP ( 'NONE', ( #36057, #70047, #32419, #71492 ) ) ;
#16138=CARTESIAN_POINT ( 'NONE',  ( -80.62287095715005592, -24.99132157543084531, 2.256160258750667502 ) ) ;
#16141=ORIENTED_EDGE ( 'NONE', *, *, #6099, .T. ) ;
#16142=CARTESIAN_POINT ( 'NONE',  ( 20.45381123341165619, -5.387677532796200097, 11.49999999999998934 ) ) ;
#16144=CARTESIAN_POINT ( 'NONE',  ( -51.87944994387085274, -25.26040897669429697, 6.553577496112825251 ) ) ;
#16145=VECTOR ( 'NONE', #64053, 1000.000000000000114 ) ;
#16146=CARTESIAN_POINT ( 'NONE',  ( -121.6259254375848400, -23.96119346886880663, -0.6495511937832033622 ) ) ;
#16147=CARTESIAN_POINT ( 'NONE',  ( -109.5228709571500474, -24.66019654487200086, 8.947790411086119278 ) ) ;
#16149=CARTESIAN_POINT ( 'NONE',  ( -18.12599551585701008, -12.76988789260850332, -1.500000000000002220 ) ) ;
#16153=CARTESIAN_POINT ( 'NONE',  ( -37.65704668824173496, -23.73766607897671221, -1.055555164236442023 ) ) ;
#16154=CARTESIAN_POINT ( 'NONE',  ( -126.5555567441935523, -24.15543982623907482, -0.2315651400026573492 ) ) ;
#16158=VECTOR ( 'NONE', #21225, 1000.000000000000114 ) ;
#16159=CARTESIAN_POINT ( 'NONE',  ( 13.32768686175602646, -14.16729652289716057, 11.49999999999998934 ) ) ;
#16160=AXIS2_PLACEMENT_3D ( 'NONE', #594, #1105, #62006 ) ;
#16161=CARTESIAN_POINT ( 'NONE',  ( -19.04320821261859464, -9.809917703373946196, 11.49999999999998934 ) ) ;
#16162=CARTESIAN_POINT ( 'NONE',  ( -62.50439628441560558, -24.15543982623907482, -0.2315651400026649265 ) ) ;
#16165=CARTESIAN_POINT ( 'NONE',  ( -101.3603016561062589, -25.18440155020230975, 3.955748670072496864 ) ) ;
#16166=CARTESIAN_POINT ( 'NONE',  ( -10.49914784070103124, -20.09245350529190688, -1.500000000000002220 ) ) ;
#16167=B_SPLINE_CURVE_WITH_KNOTS ( 'NONE', 3,
 ( #43588, #43094, #11134, #35968, #97372, #65948 ),
 .UNSPECIFIED., .F., .F.,
 ( 4, 2, 4 ),
 ( 0.000000000000000000, 0.001380764517854769086, 0.002761529035709538171 ),
 .UNSPECIFIED. ) ;
#16169=LINE ( 'NONE', #8061, #17457 ) ;
#16170=CARTESIAN_POINT ( 'NONE',  ( -72.92287095715006728, -23.47593901973090169, -1.443836447538997536 ) ) ;
#16171=CARTESIAN_POINT ( 'NONE',  ( 19.67252036444665109, 2.607452956813616218, 11.49999999999999645 ) ) ;
#16172=CARTESIAN_POINT ( 'NONE',  ( -123.5198832471558319, -24.35071581493544457, 9.817618358456016381 ) ) ;
#16174=CARTESIAN_POINT ( 'NONE',  ( -112.5895376238167245, -23.47596703998600631, 11.44779298504227683 ) ) ;
#16177=CARTESIAN_POINT ( 'NONE',  ( -49.44452229720325676, -25.19195431728568124, 6.661645827231685857 ) ) ;
#16178=CARTESIAN_POINT ( 'NONE',  ( -111.6228709571500559, -29.50247984919015209, -1.443849546365048253 ) ) ;
#16179=CARTESIAN_POINT ( 'NONE',  ( -71.52287095715004739, -24.33927499327855415, 9.819080762295804732 ) ) ;
#16180=CARTESIAN_POINT ( 'NONE',  ( -19.97641003480726241, 8.421946895145676848, -1.500000000000002220 ) ) ;
#16181=CARTESIAN_POINT ( 'NONE',  ( -56.62367364272508752, -24.66019654487199375, 8.947790411086122830 ) ) ;
#16182=CARTESIAN_POINT ( 'NONE',  ( 6.171429453590791425, 18.48145409631445446, -1.500000000000002220 ) ) ;
#16185=CARTESIAN_POINT ( 'NONE',  ( -20.10423522397153562, 3.301153050299447056, 11.49999999999999645 ) ) ;
#16186=CARTESIAN_POINT ( 'NONE',  ( -80.54559260964333589, -24.52300882791530157, 0.6510814631126378149 ) ) ;
#16187=CARTESIAN_POINT ( 'NONE',  ( -31.52287095715004739, -23.48783264083373723, -1.443836473376154617 ) ) ;
#16188=ADVANCED_FACE ( 'NONE', ( #15695 ), #84702, .T. ) ;
#16190=CARTESIAN_POINT ( 'NONE',  ( -40.52088419996039903, -25.19528773117446363, 3.295766490768270884 ) ) ;
#16191=DIRECTION ( 'NONE',  ( 0.000000000000000000, -2.173523156925980399E-06, 0.9999999999976378895 ) ) ;
#16192=CARTESIAN_POINT ( 'NONE',  ( -49.03252113942349411, -25.25214557872430277, 5.540384592041287526 ) ) ;
#16193=CARTESIAN_POINT ( 'NONE',  ( -40.57482057333878345, -24.92592662359561118, 8.075495903017996469 ) ) ;
#16194=CARTESIAN_POINT ( 'NONE',  ( -127.6228709571500559, -23.47596703998600631, 11.44779298504227860 ) ) ;
#16195=CARTESIAN_POINT ( 'NONE',  ( -0.3114230556345199963, -20.10660241673355486, 11.49999999999998934 ) ) ;
#16197=ORIENTED_EDGE ( 'NONE', *, *, #47477, .T. ) ;
#16200=EDGE_CURVE ( 'NONE', #29911, #81363, #47620, .T. ) ;
#16201=B_SPLINE_CURVE_WITH_KNOTS ( 'NONE', 3,
 ( #20616, #83009, #4414, #68300 ),
 .UNSPECIFIED., .F., .F.,
 ( 4, 4 ),
 ( 0.000000000000000000, 0.002134615384615373701 ),
 .UNSPECIFIED. ) ;
#16202=ADVANCED_FACE ( 'NONE', ( #30919 ), #97078, .T. ) ;
#16203=CARTESIAN_POINT ( 'NONE',  ( 19.82229641098322404, 11.46754112681587046, 11.49999999999999645 ) ) ;
#16204=CARTESIAN_POINT ( 'NONE',  ( -21.73129956901698989, 6.668506094012985663, 11.49999999999998934 ) ) ;
#16205=ORIENTED_EDGE ( 'NONE', *, *, #87644, .T. ) ;
#16206=CARTESIAN_POINT ( 'NONE',  ( -81.26889778654310703, -25.32614216758069503, 4.442629388656409439 ) ) ;
#16207=CARTESIAN_POINT ( 'NONE',  ( -97.52287095715007581, -23.47593901973090524, -1.443836447538996648 ) ) ;
#16209=ADVANCED_FACE ( 'NONE', ( #68984 ), #99908, .T. ) ;
#16210=CARTESIAN_POINT ( 'NONE',  ( -49.52287095715006870, -24.51283580621365132, 0.6167428607019690423 ) ) ;
#16215=AXIS2_PLACEMENT_3D ( 'NONE', #93468, #33588, #8249 ) ;
#16216=CARTESIAN_POINT ( 'NONE',  ( 11.27307661227339430, 16.98952936956587934, -1.500000000000002220 ) ) ;
#16219=CARTESIAN_POINT ( 'NONE',  ( -10.52143791818333085, 20.43947972196396989, 11.49999999999998934 ) ) ;
#16224=CARTESIAN_POINT ( 'NONE',  ( -108.5942905997697636, -23.73791477778912196, 11.05961554403169878 ) ) ;
#16226=VECTOR ( 'NONE', #54733, 1000.000000000000114 ) ;
#16227=CARTESIAN_POINT ( 'NONE',  ( -53.53686286912871140, -24.51419770103157347, 9.386484678747180510 ) ) ;
#16228=CARTESIAN_POINT ( 'NONE',  ( 0.2649960030224881025, 21.33594185153759426, 11.49999999999999645 ) ) ;
#16231=ORIENTED_EDGE ( 'NONE', *, *, #14652, .T. ) ;
#16232=CARTESIAN_POINT ( 'NONE',  ( 21.93305185196877360, -3.456643806985262302, -1.500000000000002220 ) ) ;
#16233=CARTESIAN_POINT ( 'NONE',  ( 15.34805171112899203, -13.82090413600154299, -1.500000000000002220 ) ) ;
#16234=ADVANCED_FACE ( 'NONE', ( #22787 ), #54279, .F. ) ;
#16235=VECTOR ( 'NONE', #50369, 1000.000000000000114 ) ;
#16236=ORIENTED_EDGE ( 'NONE', *, *, #8741, .F. ) ;
#16238=B_SPLINE_CURVE_WITH_KNOTS ( 'NONE', 3,
 ( #51210, #57838, #12636, #5029 ),
 .UNSPECIFIED., .F., .F.,
 ( 4, 4 ),
 ( 0.7593203366958898304, 0.7603210837366550789 ),
 .UNSPECIFIED. ) ;
#16239=CARTESIAN_POINT ( 'NONE',  ( -68.92091305805531931, -25.32724624944561853, 4.398071659717722959 ) ) ;
#16241=EDGE_LOOP ( 'NONE', ( #13707, #76487, #88945, #43071 ) ) ;
#16242=CARTESIAN_POINT ( 'NONE',  ( -51.62287095715007723, -24.35013146730202394, 9.818937971375115481 ) ) ;
#16243=ORIENTED_EDGE ( 'NONE', *, *, #28753, .T. ) ;
#16245=CARTESIAN_POINT ( 'NONE',  ( -48.52287095715009002, -24.33832256527049154, 0.1851278514138615938 ) ) ;
#16246=CARTESIAN_POINT ( 'NONE',  ( 8.468106961216914641, 19.09613275528424836, -1.500000000000002220 ) ) ;
#16247=CARTESIAN_POINT ( 'NONE',  ( -13.95179422449595208, 16.79422078803934326, 11.49999999999999645 ) ) ;
#16248=EDGE_CURVE ( 'NONE', #75416, #67086, #68490, .T. ) ;
#16249=B_SPLINE_CURVE_WITH_KNOTS ( 'NONE', 3,
 ( #92146, #16516, #84537, #63222 ),
 .UNSPECIFIED., .F., .F.,
 ( 4, 4 ),
 ( 0.000000000000000000, 9.999999999998897304E-05 ),
 .UNSPECIFIED. ) ;
#16250=CARTESIAN_POINT ( 'NONE',  ( -27.61674701359889639, -24.89280003310657108, 7.602796328702011941 ) ) ;
#16251=CARTESIAN_POINT ( 'NONE',  ( -98.90291818520829281, -25.23555723607559997, 6.309050697855190570 ) ) ;
#16252=CARTESIAN_POINT ( 'NONE',  ( 22.44084908143146251, -0.7541981612834567361, 11.49999999999998934 ) ) ;
#16253=EDGE_CURVE ( 'NONE', #57780, #84750, #39034, .T. ) ;
#16254=CARTESIAN_POINT ( 'NONE',  ( -118.5879162516116168, -24.66019654487199730, 8.947790411086115725 ) ) ;
#16255=CARTESIAN_POINT ( 'NONE',  ( -87.52287095715006160, -23.48783264083352762, -1.443836473376473695 ) ) ;
#16258=ORIENTED_EDGE ( 'NONE', *, *, #33885, .F. ) ;
#16259=EDGE_CURVE ( 'NONE', #48203, #32532, #49953, .T. ) ;
#16261=CARTESIAN_POINT ( 'NONE',  ( -18.60337119584764665, 10.53494341765418874, -1.500000000000002220 ) ) ;
#16262=CARTESIAN_POINT ( 'NONE',  ( 20.54922051473491607, -8.805037660420627077, 11.49999999999999645 ) ) ;
#16264=CARTESIAN_POINT ( 'NONE',  ( 21.00884048613226440, 1.293913838035418040, 11.49999999999998934 ) ) ;
#16265=CARTESIAN_POINT ( 'NONE',  ( -30.42620999589370356, -24.66174847805420001, 1.095666116063856776 ) ) ;
#16266=CARTESIAN_POINT ( 'NONE',  ( 18.23660095519748481, -8.086948576924280374, -1.500000000000002220 ) ) ;
#16267=CARTESIAN_POINT ( 'NONE',  ( -50.63516635189558457, -24.63419186844610564, 9.035850630976916875 ) ) ;
#16268=CARTESIAN_POINT ( 'NONE',  ( -43.52287095715008292, -24.35013146730203815, 9.818937971375106599 ) ) ;
#16269=CARTESIAN_POINT ( 'NONE',  ( -19.92591009635028243, 9.278653061003369729, -1.500000000000002220 ) ) ;
#16270=CARTESIAN_POINT ( 'NONE',  ( -87.52287095715007581, -24.50216790748205398, 0.6166512839542537261 ) ) ;
#16274=CARTESIAN_POINT ( 'NONE',  ( 3.748101851616784774, 20.49759516964078188, 11.49999999999999645 ) ) ;
#16277=CARTESIAN_POINT ( 'NONE',  ( -56.52287095715009002, -23.48783264082476308, -1.443836473390091690 ) ) ;
#16278=CARTESIAN_POINT ( 'NONE',  ( -21.31669061289120037, -0.5855882196083471714, 11.49999999999998934 ) ) ;
#16279=CARTESIAN_POINT ( 'NONE',  ( -98.51906314342498661, -23.73791477778912196, 11.05961554403170588 ) ) ;
#16280=CARTESIAN_POINT ( 'NONE',  ( -66.58953762381673869, -23.47596703998600276, 11.44779298504227505 ) ) ;
#16282=CARTESIAN_POINT ( 'NONE',  ( -31.92287095715005307, -23.47596703998600276, 11.44779298504227683 ) ) ;
#16283=CARTESIAN_POINT ( 'NONE',  ( -70.65368560070751869, -25.28687673834294003, 5.910757521653128066 ) ) ;
#16284=CARTESIAN_POINT ( 'NONE',  ( 17.90692129536829924, 13.62026984716248101, -1.500000000000002220 ) ) ;
#16286=VERTEX_POINT ( 'NONE', #57289 ) ;
#16287=CARTESIAN_POINT ( 'NONE',  ( -78.97939175184666283, -25.29137798281832872, 5.597646679547159110 ) ) ;
#16288=CARTESIAN_POINT ( 'NONE',  ( -31.54519140916136521, -24.15620529776627379, 10.23563542870661536 ) ) ;
#16289=CARTESIAN_POINT ( 'NONE',  ( -9.502044936771568473, -17.27029980899984452, 11.49999999999999645 ) ) ;
#16290=CARTESIAN_POINT ( 'NONE',  ( -125.6228709571500559, -24.15431212366393154, -0.2830839119429250372 ) ) ;
#16292=ORIENTED_EDGE ( 'NONE', *, *, #90031, .T. ) ;
#16293=CARTESIAN_POINT ( 'NONE',  ( -99.54829949207251616, -24.51314013834316796, 0.6176544820404243907 ) ) ;
#16295=CARTESIAN_POINT ( 'NONE',  ( -99.94284412489217573, -25.31439557162453369, 5.308582698213717421 ) ) ;
#16296=CARTESIAN_POINT ( 'NONE',  ( -123.5228709571500616, -23.48786465467242479, 11.44779295918253759 ) ) ;
#16297=CARTESIAN_POINT ( 'NONE',  ( 8.221391366598689743, 17.94232518691122635, 11.49999999999998934 ) ) ;
#16298=AXIS2_PLACEMENT_3D ( 'NONE', #15399, #38240, #53988 ) ;
#16299=ORIENTED_EDGE ( 'NONE', *, *, #54274, .F. ) ;
#16302=AXIS2_PLACEMENT_3D ( 'NONE', #20155, #88688, #73461 ) ;
#16304=ORIENTED_EDGE ( 'NONE', *, *, #77577, .F. ) ;
#16305=DIRECTION ( 'NONE',  ( -0.000000000000000000, 2.173523156925979552E-06, -0.9999999999976378895 ) ) ;
#16306=CARTESIAN_POINT ( 'NONE',  ( -53.62287095715004170, -23.94994826722514958, -0.6494450866351740848 ) ) ;
#16308=CARTESIAN_POINT ( 'NONE',  ( -66.52287095715007581, -23.72747288104470087, -1.053458166803226792 ) ) ;
#16310=ADVANCED_FACE ( 'NONE', ( #2484 ), #70997, .T. ) ;
#16311=CARTESIAN_POINT ( 'NONE',  ( -94.62287095715005592, -24.65952944569304606, 1.056160979905700348 ) ) ;
#16313=CARTESIAN_POINT ( 'NONE',  ( -43.52287095715006160, -23.48786465467240347, 11.44779295918255180 ) ) ;
#16314=CARTESIAN_POINT ( 'NONE',  ( -11.57650325489309395, -16.32560983125179277, 11.49999999999998934 ) ) ;
#16316=CARTESIAN_POINT ( 'NONE',  ( -99.38436720317001516, -25.27532962555875784, 3.296897355697630871 ) ) ;
#16319=EDGE_CURVE ( 'NONE', #60391, #57062, #64533, .T. ) ;
#16321=CARTESIAN_POINT ( 'NONE',  ( -109.3965479632025080, -25.18430294384156554, 3.940680077104115941 ) ) ;
#16322=CARTESIAN_POINT ( 'NONE',  ( -120.6228709571500843, -24.52232992886364471, 0.6492154411906172484 ) ) ;
#16323=CARTESIAN_POINT ( 'NONE',  ( -101.8161100070499714, -25.25287247409161040, 6.236250661346399049 ) ) ;
#16324=CARTESIAN_POINT ( 'NONE',  ( -27.68651082257923335, -24.77145582263907286, 2.274903367125437281 ) ) ;
#16325=CARTESIAN_POINT ( 'NONE',  ( -51.70072539166533687, -25.26279899730468159, 3.987152082073251780 ) ) ;
#16329=EDGE_LOOP ( 'NONE', ( #63622, #25951, #46193, #96869 ) ) ;
#16330=CARTESIAN_POINT ( 'NONE',  ( -11.07518157712430096, -17.02944518001645946, -1.500000000000002220 ) ) ;
#16332=CARTESIAN_POINT ( 'NONE',  ( -129.6228709571500417, -29.50250786944525672, 11.44777988621622633 ) ) ;
#16333=ORIENTED_EDGE ( 'NONE', *, *, #1623, .T. ) ;
#16334=PLANE ( 'NONE',  #3211 ) ;
#16335=CARTESIAN_POINT ( 'NONE',  ( 3.569899647507075890, 19.86734082857295647, -1.500000000000002220 ) ) ;
#16336=CARTESIAN_POINT ( 'NONE',  ( 20.98173926746349238, 2.650078317256617577, 11.49999999999999645 ) ) ;
#16337=CARTESIAN_POINT ( 'NONE',  ( 1.014068502963303864, -22.09113584270698993, -1.500000000000002220 ) ) ;
#16338=VECTOR ( 'NONE', #17034, 1000.000000000000114 ) ;
#16339=CARTESIAN_POINT ( 'NONE',  ( -12.99546161633903552, -15.93940442571882876, -1.500000000000002220 ) ) ;
#16340=B_SPLINE_CURVE_WITH_KNOTS ( 'NONE', 3,
 ( #18720, #51185, #27347, #20715, #5004, #4014 ),
 .UNSPECIFIED., .F., .F.,
 ( 4, 2, 4 ),
 ( 1.570755371634190273E-05, 0.001396183895866088404, 0.002776660238015835145 ),
 .UNSPECIFIED. ) ;
#16341=CARTESIAN_POINT ( 'NONE',  ( -60.48803809078037119, -24.73486907724917572, 1.287355809206962576 ) ) ;
#16345=CARTESIAN_POINT ( 'NONE',  ( -99.52287095715006160, -24.64965694238407323, 8.947790433994194714 ) ) ;
#16346=CARTESIAN_POINT ( 'NONE',  ( -61.62287095715005592, -23.96177878511308634, 10.65340807706330573 ) ) ;
#16348=EDGE_LOOP ( 'NONE', ( #72393, #89634, #26191, #56058 ) ) ;
#16349=VERTEX_POINT ( 'NONE', #2992 ) ;
#16353=CARTESIAN_POINT ( 'NONE',  ( 14.37238272058661259, 14.81585024043302035, -1.500000000000002220 ) ) ;
#16354=CARTESIAN_POINT ( 'NONE',  ( 15.89274262425319861, 14.76810421718133171, 11.49999999999999645 ) ) ;
#16355=EDGE_LOOP ( 'NONE', ( #65830, #31142, #63404, #48036 ) ) ;
#16356=CARTESIAN_POINT ( 'NONE',  ( -100.5562042904833930, -23.47596703998600631, 11.44779298504227683 ) ) ;
#16357=CARTESIAN_POINT ( 'NONE',  ( -60.62287095715004881, -24.14321612903115977, -0.2833117244521707323 ) ) ;
#16358=CARTESIAN_POINT ( 'NONE',  ( -7.019573500991415749, 21.25910006591672996, -1.500000000000002220 ) ) ;
#16360=CARTESIAN_POINT ( 'NONE',  ( -79.34687923781920915, -25.27874842775003117, 5.960409258949917799 ) ) ;
#16361=FACE_OUTER_BOUND ( 'NONE', #79524, .T. ) ;
#16362=VERTEX_POINT ( 'NONE', #25813 ) ;
#16363=DIRECTION ( 'NONE',  ( 0.000000000000000000, 2.173523156925980399E-06, -0.9999999999976378895 ) ) ;
#16365=CARTESIAN_POINT ( 'NONE',  ( -35.53620344211212512, -24.52399227489126687, 9.353111116836519301 ) ) ;
#16368=ADVANCED_FACE ( 'NONE', ( #16692 ), #56783, .T. ) ;
#16371=CARTESIAN_POINT ( 'NONE',  ( -50.62287095715010565, -24.82576562982392687, 8.398263435472973271 ) ) ;
#16372=CARTESIAN_POINT ( 'NONE',  ( -3.044128750896296420, -20.94304649679510888, -1.500000000000002220 ) ) ;
#16373=EDGE_LOOP ( 'NONE', ( #73419, #69812, #28239, #99376 ) ) ;
#16374=CARTESIAN_POINT ( 'NONE',  ( -50.53592633393567013, -24.63355581998386867, 0.9682620441943859957 ) ) ;
#16375=CARTESIAN_POINT ( 'NONE',  ( -21.01659442711627790, -5.882202039844940167, -1.500000000000002220 ) ) ;
#16376=DIRECTION ( 'NONE',  ( -3.773278334453079030E-23, 0.9999999999976377785, 2.173523156925979128E-06 ) ) ;
#16378=DIRECTION ( 'NONE',  ( 0.000000000000000000, -0.9999999999976377785, -2.173523156925979975E-06 ) ) ;
#16379=CARTESIAN_POINT ( 'NONE',  ( 11.26692973276593968, -18.67385317477220497, -1.500000000000002220 ) ) ;
#16381=ORIENTED_EDGE ( 'NONE', *, *, #32898, .F. ) ;
#16383=CARTESIAN_POINT ( 'NONE',  ( -85.59143639821803617, -24.40133493613049964, 9.663955038902802386 ) ) ;
#16384=B_SPLINE_CURVE_WITH_KNOTS ( 'NONE', 3,
 ( #374, #92709, #15590, #9488 ),
 .UNSPECIFIED., .F., .F.,
 ( 4, 4 ),
 ( 0.6602573981240899004, 0.6692638293962055451 ),
 .UNSPECIFIED. ) ;
#16385=EDGE_LOOP ( 'NONE', ( #9498, #42490, #49873, #73061 ) ) ;
#16387=ORIENTED_EDGE ( 'NONE', *, *, #77382, .T. ) ;
#16389=CARTESIAN_POINT ( 'NONE',  ( -86.62287095715004170, -23.47593901973091235, -1.443836447539002865 ) ) ;
#16390=CARTESIAN_POINT ( 'NONE',  ( 20.41123533131232648, 5.719371238976541427, -1.500000000000002220 ) ) ;
#16391=CARTESIAN_POINT ( 'NONE',  ( -94.63332968182956506, -23.96119346886881019, -0.6495511937832051386 ) ) ;
#16392=CARTESIAN_POINT ( 'NONE',  ( -79.10019335338344604, -25.27791785562742533, 6.701028845095781783 ) ) ;
#16394=LINE ( 'NONE', #10295, #50798 ) ;
#16395=CARTESIAN_POINT ( 'NONE',  ( 18.72033823704212097, 5.060218808788302880, -1.500000000000002220 ) ) ;
#16396=CARTESIAN_POINT ( 'NONE',  ( -69.34303308397305443, -25.25559839591755207, 6.209207386190695566 ) ) ;
#16398=CARTESIAN_POINT ( 'NONE',  ( -14.81708852449743929, -12.69844354874750181, 11.49999999999999645 ) ) ;
#16399=CARTESIAN_POINT ( 'NONE',  ( -45.62287095715004881, -25.00182538069145011, 7.747789668545099317 ) ) ;
#16400=CARTESIAN_POINT ( 'NONE',  ( -79.78457243948635380, -25.16093448558851620, 6.875308263077232418 ) ) ;
#16404=PLANE ( 'NONE',  #82833 ) ;
#16405=CARTESIAN_POINT ( 'NONE',  ( -93.55475863340156195, -23.96169478059713853, 10.65365249895717348 ) ) ;
#16406=CARTESIAN_POINT ( 'NONE',  ( -11.90832679833862073, -15.64659449181510986, 11.49999999999998934 ) ) ;
#16407=CARTESIAN_POINT ( 'NONE',  ( -117.6228709571501270, -24.35013146730205236, 9.818937971375103047 ) ) ;
#16408=ORIENTED_EDGE ( 'NONE', *, *, #75076, .F. ) ;
#16409=CARTESIAN_POINT ( 'NONE',  ( 20.07693369621832602, 7.961103810760662647, 11.49999999999998934 ) ) ;
#16410=CARTESIAN_POINT ( 'NONE',  ( -40.55015522979748255, -24.15503026093912453, -0.2815557561904605821 ) ) ;
#16412=CARTESIAN_POINT ( 'NONE',  ( -43.62287095715004881, -24.64898659630367206, 1.056161002820819261 ) ) ;
#16415=CARTESIAN_POINT ( 'NONE',  ( -56.52287095715006870, -23.47596703998600631, 11.44779298504228926 ) ) ;
#16420=FACE_OUTER_BOUND ( 'NONE', #80895, .T. ) ;
#16422=CARTESIAN_POINT ( 'NONE',  ( -68.52287095715006160, -23.47596703998600631, 11.44779298504228748 ) ) ;
#16423=CARTESIAN_POINT ( 'NONE',  ( 1.402406813841059030, 19.88454085074057076, 11.49999999999998934 ) ) ;
#16426=CARTESIAN_POINT ( 'NONE',  ( -0.3680779360730609406, 19.82951397037014729, -1.500000000000002220 ) ) ;
#16428=EDGE_CURVE ( 'NONE', #46879, #52307, #66889, .T. ) ;
#16432=CARTESIAN_POINT ( 'NONE',  ( -40.25203966287474344, -25.10925593919035492, 2.839407324615607298 ) ) ;
#16433=CARTESIAN_POINT ( 'NONE',  ( -35.62287095715008434, -24.82576562982393398, 8.398263435472959060 ) ) ;
#16434=CARTESIAN_POINT ( 'NONE',  ( -0.3852054317258338245, -20.75737367715079174, 11.49999999999999645 ) ) ;
#16437=CARTESIAN_POINT ( 'NONE',  ( -106.6282284235315245, -24.15543982623907127, -0.2315651400026576268 ) ) ;
#16438=CARTESIAN_POINT ( 'NONE',  ( -7.601706241105644857, -21.46296766604531570, 11.49999999999999645 ) ) ;
#16439=ORIENTED_EDGE ( 'NONE', *, *, #85079, .F. ) ;
#16440=CARTESIAN_POINT ( 'NONE',  ( -57.62287095715007723, -24.34917612406837861, 0.1852690917426648154 ) ) ;
#16443=CARTESIAN_POINT ( 'NONE',  ( 12.43249465596513126, -15.92577207200969092, 11.49999999999998934 ) ) ;
#16444=EDGE_CURVE ( 'NONE', #17917, #52403, #42556, .T. ) ;
#16445=DIRECTION ( 'NONE',  ( -3.773278334453079618E-23, 0.9999999999976377785, 2.173523156925979975E-06 ) ) ;
#16448=DIRECTION ( 'NONE',  ( 0.000000000000000000, -2.173523156925979552E-06, 0.9999999999976378895 ) ) ;
#16449=CARTESIAN_POINT ( 'NONE',  ( -18.54830753475928518, 13.48922247889305837, 11.49999999999998934 ) ) ;
#16450=PLANE ( 'NONE',  #69762 ) ;
#16451=CARTESIAN_POINT ( 'NONE',  ( 13.31326451270642330, 17.06472021985377552, -1.500000000000002220 ) ) ;
#16453=CARTESIAN_POINT ( 'NONE',  ( 2.313481123293766206, -20.83243486019555135, 11.49999999999999645 ) ) ;
#16455=CARTESIAN_POINT ( 'NONE',  ( -107.6228709571500843, -23.72773821059536559, 11.05748984161097503 ) ) ;
#16456=CARTESIAN_POINT ( 'NONE',  ( -115.2228709571500787, -23.47596703998600631, 11.44779298504227860 ) ) ;
#16457=CARTESIAN_POINT ( 'NONE',  ( -10.85839155550747392, 19.17434714687634667, -1.500000000000002220 ) ) ;
#16458=CARTESIAN_POINT ( 'NONE',  ( -124.4728709571500360, -25.21113200442380275, 5.000950865234349507 ) ) ;
#16463=VERTEX_POINT ( 'NONE', #27312 ) ;
#16464=CARTESIAN_POINT ( 'NONE',  ( -123.6228709571500559, -24.64965695001469115, 8.947790433994175174 ) ) ;
#16465=ORIENTED_EDGE ( 'NONE', *, *, #13837, .T. ) ;
#16468=CARTESIAN_POINT ( 'NONE',  ( -83.52287095715013265, -24.33927499327856125, 9.819080762295813614 ) ) ;
#16469=CARTESIAN_POINT ( 'NONE',  ( -36.57553010991347264, -24.65952944569304606, 1.056160979905696129 ) ) ;
#16470=CARTESIAN_POINT ( 'NONE',  ( 18.57849760351508195, 8.651319581928444080, -1.500000000000002220 ) ) ;
#16471=EDGE_CURVE ( 'NONE', #23306, #45965, #50653, .T. ) ;
#16472=ORIENTED_EDGE ( 'NONE', *, *, #15418, .F. ) ;
#16473=CARTESIAN_POINT ( 'NONE',  ( -116.5895376238167103, -24.66019654487199375, 8.947790411086122830 ) ) ;
#16474=CARTESIAN_POINT ( 'NONE',  ( -44.62370635163588872, -24.65952944569304606, 1.056160979905693909 ) ) ;
#16476=CARTESIAN_POINT ( 'NONE',  ( 22.08996893241407378, 3.065900275835479860, 11.49999999999998934 ) ) ;
#16477=ADVANCED_FACE ( 'NONE', ( #65407 ), #3984, .T. ) ;
#16478=CARTESIAN_POINT ( 'NONE',  ( -55.52287095715006870, -25.00182538069145011, 7.747789668545106423 ) ) ;
#16480=ORIENTED_EDGE ( 'NONE', *, *, #29880, .F. ) ;
#16481=CARTESIAN_POINT ( 'NONE',  ( -29.03649758528140623, -24.85412015691543530, 2.179221534033828345 ) ) ;
#16483=CARTESIAN_POINT ( 'NONE',  ( -17.75621389795859884, -10.86975384844714831, -1.500000000000002220 ) ) ;
#16485=ORIENTED_EDGE ( 'NONE', *, *, #20226, .T. ) ;
#16488=VERTEX_POINT ( 'NONE', #34926 ) ;
#16489=CARTESIAN_POINT ( 'NONE',  ( -51.21833214457227257, -25.12217806580932944, 6.843755411117837362 ) ) ;
#16490=CARTESIAN_POINT ( 'NONE',  ( 4.154569570224219355, 20.57273982587956240, -1.500000000000002220 ) ) ;
#16494=CARTESIAN_POINT ( 'NONE',  ( -37.52287095715009713, -24.33927499327855770, 9.819080762295813614 ) ) ;
#16498=CARTESIAN_POINT ( 'NONE',  ( -65.62287095715001328, -24.83620972994592080, 8.398175272781363887 ) ) ;
#16499=CARTESIAN_POINT ( 'NONE',  ( -22.11188964843745453, -1.696007508606716341, 11.49999999999999645 ) ) ;
#16500=VERTEX_POINT ( 'NONE', #90205 ) ;
#16501=CARTESIAN_POINT ( 'NONE',  ( -98.89303308397306580, -25.26498937201382233, 6.110950154240443410 ) ) ;
#16502=EDGE_CURVE ( 'NONE', #66705, #94640, #69345, .T. ) ;
#16503=CARTESIAN_POINT ( 'NONE',  ( -44.62287095715007013, -24.35013146730203104, 9.818937971375117257 ) ) ;
#16504=EDGE_LOOP ( 'NONE', ( #48354, #76157, #73645, #2294 ) ) ;
#16505=CARTESIAN_POINT ( 'NONE',  ( -19.66899025692886838, 11.29834648773183581, -1.500000000000002220 ) ) ;
#16506=LINE ( 'NONE', #33753, #62019 ) ;
#16507=ORIENTED_EDGE ( 'NONE', *, *, #9563, .T. ) ;
#16508=AXIS2_PLACEMENT_3D ( 'NONE', #24671, #2359, #87081 ) ;
#16513=CARTESIAN_POINT ( 'NONE',  ( -11.96439459519798554, -16.23097265130270728, -1.500000000000002220 ) ) ;
#16514=DIRECTION ( 'NONE',  ( -3.773278334453079030E-23, 0.9999999999976377785, 2.173523156925979128E-06 ) ) ;
#16515=ORIENTED_EDGE ( 'NONE', *, *, #94557, .F. ) ;
#16516=CARTESIAN_POINT ( 'NONE',  ( -39.58953762381673158, -23.48786465467240347, 11.44779295918255180 ) ) ;
#16517=CARTESIAN_POINT ( 'NONE',  ( -15.72835732567950195, 15.92727474065614501, -1.500000000000002220 ) ) ;
#16520=PLANE ( 'NONE',  #43339 ) ;
#16522=CARTESIAN_POINT ( 'NONE',  ( -40.11011405477550795, -25.31552197567200224, 5.046770785554223870 ) ) ;
#16525=CARTESIAN_POINT ( 'NONE',  ( 2.036066721924049805, 19.47704226162102614, 11.49999999999998934 ) ) ;
#16527=ORIENTED_EDGE ( 'NONE', *, *, #79840, .T. ) ;
#16528=CARTESIAN_POINT ( 'NONE',  ( 13.13055478438326773, -17.03443908202477886, -1.500000000000002220 ) ) ;
#16530=CARTESIAN_POINT ( 'NONE',  ( -121.5228709571501042, -23.48783264082477018, -1.443836473390083253 ) ) ;
#16531=CARTESIAN_POINT ( 'NONE',  ( -129.5228709571501042, -24.51387760970725793, 9.387446482453407626 ) ) ;
#16532=CARTESIAN_POINT ( 'NONE',  ( -68.62287095715005592, -23.47596703998600631, 11.44779298504227505 ) ) ;
#16533=CARTESIAN_POINT ( 'NONE',  ( -17.89994474767736676, -14.32179853049041363, -1.500000000000002220 ) ) ;
#16536=CARTESIAN_POINT ( 'NONE',  ( -96.59382141558563717, -23.96169478059713498, 10.65365249895717881 ) ) ;
#16538=CARTESIAN_POINT ( 'NONE',  ( 20.02521558760690112, -0.9251608499524575091, 11.49999999999999645 ) ) ;
#16539=CARTESIAN_POINT ( 'NONE',  ( -80.21014334459538020, -25.31594316633425734, 4.508707480579172255 ) ) ;
#16540=CARTESIAN_POINT ( 'NONE',  ( -57.52287095715003318, -24.66019654487198665, 8.947790411086121054 ) ) ;
#16542=CARTESIAN_POINT ( 'NONE',  ( -119.5228709571500758, -24.64898659630368627, 1.056161002820833028 ) ) ;
#16544=ORIENTED_EDGE ( 'NONE', *, *, #34316, .T. ) ;
#16546=CARTESIAN_POINT ( 'NONE',  ( 18.41774212405765709, -11.57998961627671441, 11.49999999999998934 ) ) ;
#16547=CARTESIAN_POINT ( 'NONE',  ( -45.52287095715007581, -23.85229601348996198, 10.88205029486208986 ) ) ;
#16548=CARTESIAN_POINT ( 'NONE',  ( -5.193715590271882121, 18.98282465337476665, -1.500000000000002220 ) ) ;
#16550=CARTESIAN_POINT ( 'NONE',  ( -109.9698394925872549, -25.27925910355527250, 5.331473675041118021 ) ) ;
#16553=EDGE_CURVE ( 'NONE', #80383, #25080, #25859, .T. ) ;
#16554=CARTESIAN_POINT ( 'NONE',  ( -56.62287095715005592, -24.64965695001468404, 8.947790433994185832 ) ) ;
#16556=CARTESIAN_POINT ( 'NONE',  ( -19.32567751138619982, -7.045664331180771178, 11.49999999999999645 ) ) ;
#16557=CARTESIAN_POINT ( 'NONE',  ( -89.40841769935767047, -29.50249917535260380, 7.447779886225679213 ) ) ;
#16559=ADVANCED_FACE ( 'NONE', ( #98299 ), #66984, .T. ) ;
#16560=CARTESIAN_POINT ( 'NONE',  ( -120.6293614585003269, -23.48783264082477018, -1.443836473390085695 ) ) ;
#16561=CARTESIAN_POINT ( 'NONE',  ( -16.68516988606489448, 15.22057433622007316, 11.49999999999999645 ) ) ;
#16562=ORIENTED_EDGE ( 'NONE', *, *, #76438, .T. ) ;
#16563=( LENGTH_UNIT ( ) NAMED_UNIT ( * ) SI_UNIT ( .MILLI., .METRE. ) );
#16564=CARTESIAN_POINT ( 'NONE',  ( -99.82150581108260212, -25.31296402341794760, 4.513512821131813624 ) ) ;
#16566=CARTESIAN_POINT ( 'NONE',  ( -125.5896765834183810, -24.52399227489127043, 9.353111116836528183 ) ) ;
#16571=ORIENTED_EDGE ( 'NONE', *, *, #36633, .F. ) ;
#16573=CARTESIAN_POINT ( 'NONE',  ( -79.38647268321243189, -25.31596371128505751, 5.652477663093335991 ) ) ;
#16574=CARTESIAN_POINT ( 'NONE',  ( 4.317061085376620255, -22.40314112565372540, -1.500000000000002220 ) ) ;
#16575=CARTESIAN_POINT ( 'NONE',  ( -74.64368143928086852, -23.73766607897670511, -1.055555164236458898 ) ) ;
#16577=DIRECTION ( 'NONE',  ( -0.000000000000000000, 2.173523156925979552E-06, -0.9999999999976378895 ) ) ;
#16579=CARTESIAN_POINT ( 'NONE',  ( 5.309366582633749054, -21.77581755331916824, 11.49999999999999645 ) ) ;
#16580=EDGE_LOOP ( 'NONE', ( #27664, #19995, #85631, #98807 ) ) ;
#16581=CARTESIAN_POINT ( 'NONE',  ( -43.52287095715006160, -23.47596703998600631, 11.44779298504229281 ) ) ;
#16582=CARTESIAN_POINT ( 'NONE',  ( 21.83198049998918577, 2.282343850347359648, -1.500000000000002220 ) ) ;
#16584=CARTESIAN_POINT ( 'NONE',  ( -34.62373385991148211, -24.66019654487199730, 8.947790411086117501 ) ) ;
#16585=CARTESIAN_POINT ( 'NONE',  ( -121.5228709571500616, -23.72773821059536914, 11.05748984161097503 ) ) ;
#16586=ORIENTED_EDGE ( 'NONE', *, *, #38069, .F. ) ;
#16587=CARTESIAN_POINT ( 'NONE',  ( -48.59339690811989243, -24.15620529776627734, 10.23563542870660470 ) ) ;
#16588=CARTESIAN_POINT ( 'NONE',  ( -112.5562042904833930, -24.66019654487199730, 8.947790411086124607 ) ) ;
#16589=ORIENTED_EDGE ( 'NONE', *, *, #5547, .F. ) ;
#16590=CARTESIAN_POINT ( 'NONE',  ( -12.04554601739387998, 16.56303510970703385, -1.500000000000002220 ) ) ;
#16592=ORIENTED_EDGE ( 'NONE', *, *, #81296, .F. ) ;
#16594=ORIENTED_EDGE ( 'NONE', *, *, #5912, .F. ) ;
#16596=CARTESIAN_POINT ( 'NONE',  ( 11.92049557817732364, -19.74369927386287671, -1.500000000000002220 ) ) ;
#16598=CARTESIAN_POINT ( 'NONE',  ( -12.35269427871797987, -16.12754648828645543, -1.500000000000002220 ) ) ;
#16601=CARTESIAN_POINT ( 'NONE',  ( -37.58953762381672448, -23.48783264082477373, -1.443836473390072372 ) ) ;
#16602=EDGE_CURVE ( 'NONE', #76130, #79877, #36916, .T. ) ;
#16603=CARTESIAN_POINT ( 'NONE',  ( -46.52287095715006160, -24.65952944569304606, 1.056160979905693686 ) ) ;
#16605=CARTESIAN_POINT ( 'NONE',  ( 20.90071823198991297, 5.034746273075951351, 11.49999999999999645 ) ) ;
#16606=ORIENTED_EDGE ( 'NONE', *, *, #99793, .F. ) ;
#16607=CARTESIAN_POINT ( 'NONE',  ( -89.52287095715006160, -24.64965694238407323, 8.947790433994196491 ) ) ;
#16609=ORIENTED_EDGE ( 'NONE', *, *, #9954, .T. ) ;
#16610=CARTESIAN_POINT ( 'NONE',  ( 20.74337371777590278, 0.4424840333690017724, 11.49999999999998934 ) ) ;
#16613=CARTESIAN_POINT ( 'NONE',  ( -125.5551874828237970, -24.40034930558991633, 0.3402023900116222244 ) ) ;
#16614=ORIENTED_EDGE ( 'NONE', *, *, #27249, .F. ) ;
#16615=ADVANCED_FACE ( 'NONE', ( #69868 ), #15073, .T. ) ;
#16616=AXIS2_PLACEMENT_3D ( 'NONE', #46495, #63747, #46004 ) ;
#16617=B_SPLINE_SURFACE_WITH_KNOTS ( 'NONE', 3, 1, ( 
 ( #56784, #25307 ),
 ( #24802, #56286 ),
 ( #18201, #55782 ),
 ( #87209, #2993 ),
 ( #87719, #17700 ),
 ( #17194, #79087 ),
 ( #64910, #95819 ),
 ( #26317, #20066 ),
 ( #59143, #16693 ),
 ( #51028, #47662 ),
 ( #48162, #9589 ),
 ( #71501, #78578 ),
 ( #9085, #40038 ),
 ( #82463, #5841 ),
 ( #92068, #68743 ) ),
 .UNSPECIFIED., .F., .F., .F.,
 ( 4, 1, 1, 1, 1, 1, 1, 1, 1, 1, 1, 1, 4 ),
 ( 2, 2 ),
 ( 0.000000000000000000, 0.09831997398134753596, 0.1994174736496688582, 0.3056025976021228274, 0.4161623563557467209, 0.4745823813143021375, 0.5370064812335182403, 0.6038573606499607616, 0.6740896076918744262, 0.7494169867637917593, 0.8282534808908113000, 0.9120541595560537340, 1.000000000000000000 ),
 ( 0.000000000000000000, 1.000000000000000000 ),
 .UNSPECIFIED. ) ;
#16618=CARTESIAN_POINT ( 'NONE',  ( -75.62287095715007013, -24.51254535404255464, 9.355368623467656519 ) ) ;
#16623=B_SPLINE_CURVE_WITH_KNOTS ( 'NONE', 3,
 ( #95449, #19810, #3123, #12201 ),
 .UNSPECIFIED., .F., .F.,
 ( 4, 4 ),
 ( 0.000000000000000000, 9.999999999999592548E-05 ),
 .UNSPECIFIED. ) ;
#16624=B_SPLINE_CURVE_WITH_KNOTS ( 'NONE', 3,
 ( #46077, #76996, #30839, #23212, #54197, #86626, #40960, #32339, #26233, #56704 ),
 .UNSPECIFIED., .F., .F.,
 ( 4, 2, 2, 2, 4 ),
 ( 0.000000000000000000, 0.0001827656628061555440, 0.0003655313256123110879, 0.0005482969884184666319, 0.0007310626512246221759 ),
 .UNSPECIFIED. ) ;
#16626=B_SPLINE_CURVE_WITH_KNOTS ( 'NONE', 3,
 ( #7976, #38927, #62282, #54667 ),
 .UNSPECIFIED., .F., .F.,
 ( 4, 4 ),
 ( 0.000000000000000000, 9.999999999998897304E-05 ),
 .UNSPECIFIED. ) ;
#16627=CARTESIAN_POINT ( 'NONE',  ( -43.48232127904228150, -24.66019654487199375, 8.947790411086122830 ) ) ;
#16628=CARTESIAN_POINT ( 'NONE',  ( -7.807709442696729063, 20.60712426125841645, 11.49999999999999645 ) ) ;
#16630=CARTESIAN_POINT ( 'NONE',  ( 7.090404290683943067, 21.45231405096426514, -1.500000000000002220 ) ) ;
#16631=CARTESIAN_POINT ( 'NONE',  ( 18.73254098450790295, -9.497730595714260815, 11.49999999999998934 ) ) ;
#16633=CARTESIAN_POINT ( 'NONE',  ( -99.38771510255533315, -25.29141603707036268, 5.771832689820707962 ) ) ;
#16634=VERTEX_POINT ( 'NONE', #23169 ) ;
#16641=CARTESIAN_POINT ( 'NONE',  ( 17.61891135320703938, 11.69080507458975227, 11.49999999999998934 ) ) ;
#16643=CARTESIAN_POINT ( 'NONE',  ( -59.79060349298165278, -25.33009847151394922, 4.495758292450050320 ) ) ;
#16644=CARTESIAN_POINT ( 'NONE',  ( -121.5915913388690370, -23.73766607897670156, -1.055555164236450905 ) ) ;
#16645=B_SPLINE_CURVE_WITH_KNOTS ( 'NONE', 3,
 ( #82360, #12839, #43808, #56318, #68640, #52921 ),
 .UNSPECIFIED., .F., .F.,
 ( 4, 2, 4 ),
 ( 6.384118694780321315E-06, 0.001386860460836456411, 0.002767336802978132785 ),
 .UNSPECIFIED. ) ;
#16646=PLANE ( 'NONE',  #10302 ) ;
#16647=CARTESIAN_POINT ( 'NONE',  ( -80.62287095715005592, -23.47593901973091235, -1.443836447539004642 ) ) ;
#16648=CARTESIAN_POINT ( 'NONE',  ( 14.93699691249320693, 16.48547057857716425, -1.500000000000002220 ) ) ;
#16649=CARTESIAN_POINT ( 'NONE',  ( -114.5520207083192332, -24.51314013834316086, 0.6176544820404251679 ) ) ;
#16652=LINE ( 'NONE', #2445, #28159 ) ;
#16656=DIRECTION ( 'NONE',  ( -3.773278334453079618E-23, 0.9999999999976377785, 2.173523156925979975E-06 ) ) ;
#16658=CARTESIAN_POINT ( 'NONE',  ( -19.16120753946698585, -3.443109951913609024, 11.49999999999998934 ) ) ;
#16661=CARTESIAN_POINT ( 'NONE',  ( -20.93543047832761417, 4.563121699532205255, -1.500000000000002220 ) ) ;
#16665=CARTESIAN_POINT ( 'NONE',  ( -101.3340698065965455, -25.18440142138669202, 3.896482854220133518 ) ) ;
#16666=CARTESIAN_POINT ( 'NONE',  ( 22.70222466501550329, 0.2752559529566028229, -1.500000000000002220 ) ) ;
#16668=DIRECTION ( 'NONE',  ( -1.000000000000000000, -3.773278334444167608E-23, -8.201307833595939069E-29 ) ) ;
#16669=PLANE ( 'NONE',  #70263 ) ;
#16670=CARTESIAN_POINT ( 'NONE',  ( 18.55763160240848109, 7.024834138330111166, 11.49999999999999645 ) ) ;
#16671=CARTESIAN_POINT ( 'NONE',  ( -123.5557599765402159, -23.96169478059714564, 10.65365249895717170 ) ) ;
#16672=AXIS2_PLACEMENT_3D ( 'NONE', #89637, #98230, #12997 ) ;
#16673=CARTESIAN_POINT ( 'NONE',  ( -108.6228709571500417, -23.48786465467242479, 11.44779295918253759 ) ) ;
#16674=CARTESIAN_POINT ( 'NONE',  ( -127.5228709571500616, -23.47596703998600631, 11.44779298504227683 ) ) ;
#16678=LINE ( 'NONE', #69968, #81490 ) ;
#16679=CARTESIAN_POINT ( 'NONE',  ( -51.69862270353959843, -25.27412468278110325, 3.939198053822961398 ) ) ;
#16680=CARTESIAN_POINT ( 'NONE',  ( -20.56447267657262401, 6.860157381912782348, -1.500000000000002220 ) ) ;
#16681=CARTESIAN_POINT ( 'NONE',  ( -56.49719084987101070, -24.35071581493543391, 9.817618358456030592 ) ) ;
#16682=CARTESIAN_POINT ( 'NONE',  ( -19.06185424839875964, 3.971334347869299286, -1.500000000000002220 ) ) ;
#16683=PLANE ( 'NONE',  #74962 ) ;
#16685=CARTESIAN_POINT ( 'NONE',  ( -6.692510123977180925, 19.25193956699996178, 11.49999999999999645 ) ) ;
#16686=CARTESIAN_POINT ( 'NONE',  ( 6.026637739148365548E-17, -29.50250786944496539, 11.44777975102276635 ) ) ;
#16688=CARTESIAN_POINT ( 'NONE',  ( -95.52287095715006160, -29.50247984919015209, -1.443849546365050029 ) ) ;
#16689=EDGE_CURVE ( 'NONE', #76909, #83981, #85583, .T. ) ;
#16690=ORIENTED_EDGE ( 'NONE', *, *, #99789, .T. ) ;
#16691=LINE ( 'NONE', #47660, #45925 ) ;
#16692=FACE_OUTER_BOUND ( 'NONE', #98289, .T. ) ;
#16693=CARTESIAN_POINT ( 'NONE',  ( -39.26664729043937996, -25.27985447715197509, 5.049946080353571176 ) ) ;
#16694=CARTESIAN_POINT ( 'NONE',  ( -40.62378914844666156, -25.00182538069146787, 7.747789668545040698 ) ) ;
#16696=CARTESIAN_POINT ( 'NONE',  ( 19.67429046578372365, -4.105084037421226739, 11.49999999999998934 ) ) ;
#16698=CARTESIAN_POINT ( 'NONE',  ( -109.5201659922639550, -23.73766607897670156, -1.055555164236452903 ) ) ;
#16701=CARTESIAN_POINT ( 'NONE',  ( -66.60300861680383377, -23.73791477778911840, 11.05961554403170766 ) ) ;
#16702=EDGE_CURVE ( 'NONE', #7274, #20892, #14877, .T. ) ;
#16703=CARTESIAN_POINT ( 'NONE',  ( -22.92702450682246251, 0.3551139841105944162, 11.49999999999999645 ) ) ;
#16704=CARTESIAN_POINT ( 'NONE',  ( -18.45961786539058380, -13.25243217869837231, -1.500000000000002220 ) ) ;
#16706=CARTESIAN_POINT ( 'NONE',  ( -30.47287095715007510, -24.38330924582771786, 9.665504117595752120 ) ) ;
#16707=B_SPLINE_CURVE_WITH_KNOTS ( 'NONE', 3,
 ( #46792, #31050, #86353, #87347 ),
 .UNSPECIFIED., .F., .F.,
 ( 4, 4 ),
 ( 0.000000000000000000, 0.0001000000000000028644 ),
 .UNSPECIFIED. ) ;
#16709=CARTESIAN_POINT ( 'NONE',  ( -91.55620429048340725, -23.48786465467241769, 11.44779295918253936 ) ) ;
#16710=CARTESIAN_POINT ( 'NONE',  ( -38.56989630778316780, -23.48786465467240347, 11.44779295918255002 ) ) ;
#16711=CARTESIAN_POINT ( 'NONE',  ( -112.5228709571500616, -23.48786465467241769, 11.44779295918253936 ) ) ;
#16713=CARTESIAN_POINT ( 'NONE',  ( -55.62287095715004170, -29.50249982740957577, 7.747779886224967605 ) ) ;
#16714=CARTESIAN_POINT ( 'NONE',  ( -79.34687923781920915, -29.50249594249816099, 5.960400078536885360 ) ) ;
#16715=ORIENTED_EDGE ( 'NONE', *, *, #464, .F. ) ;
#16716=CARTESIAN_POINT ( 'NONE',  ( 17.64890103348723116, 10.21726211432410203, 11.49999999999998934 ) ) ;
#16718=CARTESIAN_POINT ( 'NONE',  ( -15.63304604236160067, -16.83380969201049382, -1.500000000000002220 ) ) ;
#16720=ORIENTED_EDGE ( 'NONE', *, *, #84712, .T. ) ;
#16725=CARTESIAN_POINT ( 'NONE',  ( -18.83571791729191958, -9.990160686573538840, 11.49999999999999645 ) ) ;
#16726=ORIENTED_EDGE ( 'NONE', *, *, #19463, .T. ) ;
#16728=CARTESIAN_POINT ( 'NONE',  ( 6.060481786824854389, 21.40074245971799627, -1.500000000000002220 ) ) ;
#16729=CARTESIAN_POINT ( 'NONE',  ( -3.285303218690974525, -20.39892020120133154, 11.49999999999998934 ) ) ;
#16731=VERTEX_POINT ( 'NONE', #11828 ) ;
#16734=CARTESIAN_POINT ( 'NONE',  ( -68.92123217116099454, -25.31392322340849432, 5.203679841770401104 ) ) ;
#16735=ORIENTED_EDGE ( 'NONE', *, *, #20038, .F. ) ;
#16739=CARTESIAN_POINT ( 'NONE',  ( -58.49328643788003745, -24.51419770103156637, 9.386484678747176957 ) ) ;
#16740=CARTESIAN_POINT ( 'NONE',  ( 3.889286922045745776, 20.52237432693057073, -1.500000000000002220 ) ) ;
#16741=CARTESIAN_POINT ( 'NONE',  ( 8.176594470695947692, -20.27425322898990601, 11.49999999999999645 ) ) ;
#16744=CARTESIAN_POINT ( 'NONE',  ( 17.87336509531889561, -13.68139028912531785, 11.49999999999998934 ) ) ;
#16745=CARTESIAN_POINT ( 'NONE',  ( -118.5530091436460509, -24.51419770103160189, 9.386484678747169852 ) ) ;
#16746=CARTESIAN_POINT ( 'NONE',  ( -57.62287095715005592, -23.94994826722515313, -0.6494450866351703100 ) ) ;
#16750=VERTEX_POINT ( 'NONE', #48548 ) ;
#16752=EDGE_LOOP ( 'NONE', ( #12009, #25635, #87042, #95479 ) ) ;
#16754=CARTESIAN_POINT ( 'NONE',  ( 6.831138157384286203, 20.27010762675863731, -1.500000000000002220 ) ) ;
#16755=CARTESIAN_POINT ( 'NONE',  ( 14.50327815619135308, -17.01817589256642194, 11.49999999999999645 ) ) ;
#16756=ORIENTED_EDGE ( 'NONE', *, *, #67096, .F. ) ;
#16757=CARTESIAN_POINT ( 'NONE',  ( -5.931750313267273533, -20.21149935180699231, -1.500000000000002220 ) ) ;
#16758=CARTESIAN_POINT ( 'NONE',  ( -61.58953762381672448, -23.47593901973091235, -1.443836447539007972 ) ) ;
#16759=CARTESIAN_POINT ( 'NONE',  ( -19.95465934538571062, -0.7993260556091378310, -1.500000000000002220 ) ) ;
#16762=CARTESIAN_POINT ( 'NONE',  ( -117.6228709571500701, -24.34917612406838217, 0.1852690917426713935 ) ) ;
#16764=CARTESIAN_POINT ( 'NONE',  ( -5.411813039392390223, -21.34095290059367755, -1.500000000000002220 ) ) ;
#16765=DIRECTION ( 'NONE',  ( -0.04171448572128191867, 0.5400267985901394674, -0.8406134417706475626 ) ) ;
#16766=VERTEX_POINT ( 'NONE', #94699 ) ;
#16768=VECTOR ( 'NONE', #58967, 1000.000000000000114 ) ;
#16770=CARTESIAN_POINT ( 'NONE',  ( -127.5562042904833646, -23.47596703998600631, 11.44779298504227683 ) ) ;
#16771=CARTESIAN_POINT ( 'NONE',  ( -18.54028579900546703, -9.471972883075929772, 11.49999999999999645 ) ) ;
#16772=EDGE_CURVE ( 'NONE', #27358, #93569, #39912, .T. ) ;
#16773=EDGE_CURVE ( 'NONE', #72803, #41185, #79049, .T. ) ;
#16775=B_SPLINE_CURVE_WITH_KNOTS ( 'NONE', 3,
 ( #21031, #81457, #42899, #35286 ),
 .UNSPECIFIED., .F., .F.,
 ( 4, 4 ),
 ( 0.000000000000000000, 0.0001000000000000028644 ),
 .UNSPECIFIED. ) ;
#16776=VECTOR ( 'NONE', #53738, 1000.000000000000114 ) ;
#16777=PLANE ( 'NONE',  #3634 ) ;
#16778=EDGE_CURVE ( 'NONE', #41074, #72641, #51202, .T. ) ;
#16780=CARTESIAN_POINT ( 'NONE',  ( -16.81368161134402683, 13.12552177539105358, -1.500000000000002220 ) ) ;
#16781=CARTESIAN_POINT ( 'NONE',  ( -29.52287095715006160, -24.56627961951908645, 8.947790480023282811 ) ) ;
#16783=PLANE ( 'NONE',  #94026 ) ;
#16785=CARTESIAN_POINT ( 'NONE',  ( -22.36795837939145670, 2.692536522722862813, -1.500000000000002220 ) ) ;
#16788=CARTESIAN_POINT ( 'NONE',  ( -80.26338284007071877, -25.29550791665888454, 4.507555199503806342 ) ) ;
#16790=CARTESIAN_POINT ( 'NONE',  ( -0.7274468246531539117, 19.66889477801398911, 11.49999999999999645 ) ) ;
#16791=CARTESIAN_POINT ( 'NONE',  ( -41.52287095715006870, -23.47593901973090169, -1.443836447538997092 ) ) ;
#16792=CARTESIAN_POINT ( 'NONE',  ( -32.52287095715003318, -24.66019654487198665, 8.947790411086131712 ) ) ;
#16794=ADVANCED_FACE ( 'NONE', ( #95206 ), #40422, .F. ) ;
#16795=VERTEX_POINT ( 'NONE', #43296 ) ;
#16800=B_SPLINE_CURVE_WITH_KNOTS ( 'NONE', 3,
 ( #24659, #71357, #25672, #8946 ),
 .UNSPECIFIED., .F., .F.,
 ( 4, 4 ),
 ( 0.000000000000000000, 1.000000000000000000 ),
 .UNSPECIFIED. ) ;
#16801=CARTESIAN_POINT ( 'NONE',  ( 6.816645498261984848, 18.52099371530728789, -1.500000000000002220 ) ) ;
#16803=CARTESIAN_POINT ( 'NONE',  ( 14.48468284575590204, 14.13777120147990729, 11.49999999999999645 ) ) ;
#16804=CARTESIAN_POINT ( 'NONE',  ( -110.0285167521317788, -25.20072809708166517, 3.334473250954808954 ) ) ;
#16805=EDGE_CURVE ( 'NONE', #69709, #79287, #90452, .T. ) ;
#16809=CARTESIAN_POINT ( 'NONE',  ( -67.62287095715012697, -23.96127896941632685, -0.6493128931037859264 ) ) ;
#16810=CARTESIAN_POINT ( 'NONE',  ( -80.51758134885872664, -25.30554031725500508, 4.968846701839494173 ) ) ;
#16811=CARTESIAN_POINT ( 'NONE',  ( -51.36075006403625309, -25.28866304528649067, 5.655890479381174174 ) ) ;
#16812=CARTESIAN_POINT ( 'NONE',  ( -67.62287095715005592, -24.64898659630367916, 1.056161002820824368 ) ) ;
#16813=CARTESIAN_POINT ( 'NONE',  ( -58.62287095715004881, -23.47593901973091235, -1.443836447539007972 ) ) ;
#16815=CARTESIAN_POINT ( 'NONE',  ( -120.6228709571500417, -29.50250243563736774, 8.947779886222134493 ) ) ;
#16816=CARTESIAN_POINT ( 'NONE',  ( 14.90458806734895703, -13.33898509196910886, 11.49999999999998934 ) ) ;
#16817=EDGE_CURVE ( 'NONE', #42155, #79844, #18478, .T. ) ;
#16820=ORIENTED_EDGE ( 'NONE', *, *, #11089, .T. ) ;
#16822=EDGE_CURVE ( 'NONE', #11930, #69195, #44010, .T. ) ;
#16823=CARTESIAN_POINT ( 'NONE',  ( -38.62287095715005592, -29.50248528299804818, 1.056150453629031594 ) ) ;
#16824=CARTESIAN_POINT ( 'NONE',  ( -109.8707484289256655, -25.18430176427498779, 3.397982113237853596 ) ) ;
#16826=CARTESIAN_POINT ( 'NONE',  ( -82.62287095715005592, -24.64965695001468404, 8.947790433994182280 ) ) ;
#16828=LINE ( 'NONE', #55914, #87483 ) ;
#16830=ADVANCED_FACE ( 'NONE', ( #5715 ), #13314, .T. ) ;
#16831=CARTESIAN_POINT ( 'NONE',  ( -101.9695858942169480, -25.20650842489795807, 6.812665538484691474 ) ) ;
#16832=ORIENTED_EDGE ( 'NONE', *, *, #92599, .T. ) ;
#16833=B_SPLINE_CURVE_WITH_KNOTS ( 'NONE', 3,
 ( #60984, #69081, #14285, #77678 ),
 .UNSPECIFIED., .F., .F.,
 ( 4, 4 ),
 ( 0.000000000000000000, 1.000000000000000000 ),
 .UNSPECIFIED. ) ;
#16834=CARTESIAN_POINT ( 'NONE',  ( -12.35269427871797987, -16.12754648828645543, 11.49999999999998934 ) ) ;
#16836=AXIS2_PLACEMENT_3D ( 'NONE', #32561, #47797, #40184 ) ;
#16837=DIRECTION ( 'NONE',  ( -3.773278334444166432E-23, 1.000000000000000000, 0.000000000000000000 ) ) ;
#16839=FACE_OUTER_BOUND ( 'NONE', #32191, .T. ) ;
#16840=CARTESIAN_POINT ( 'NONE',  ( -14.30055291515510518, -14.21740073472259525, -1.500000000000002220 ) ) ;
#16841=B_SPLINE_CURVE_WITH_KNOTS ( 'NONE', 3,
 ( #15976, #46947, #24592, #39321 ),
 .UNSPECIFIED., .F., .F.,
 ( 4, 4 ),
 ( 1.387778780781445676E-17, 0.0001000000000000028508 ),
 .UNSPECIFIED. ) ;
#16843=CARTESIAN_POINT ( 'NONE',  ( 1.812468502196824760, -21.08352789287561180, 11.49999999999999645 ) ) ;
#16844=CARTESIAN_POINT ( 'NONE',  ( -4.315754209668272168, 21.71352930684897942, 11.49999999999998934 ) ) ;
#16845=B_SPLINE_CURVE_WITH_KNOTS ( 'NONE', 3,
 ( #82921, #75311, #43880, #13411, #44384, #5308 ),
 .UNSPECIFIED., .F., .F.,
 ( 4, 2, 4 ),
 ( 0.000000000000000000, 0.001380901958385383774, 0.002761803916770767548 ),
 .UNSPECIFIED. ) ;
#16846=CARTESIAN_POINT ( 'NONE',  ( -15.41819309731374510, 13.62919173607049927, -1.500000000000002220 ) ) ;
#16849=CARTESIAN_POINT ( 'NONE',  ( -43.52287095715008292, -24.33832256527048088, 0.1851278514138565978 ) ) ;
#16850=VERTEX_POINT ( 'NONE', #50905 ) ;
#16851=CARTESIAN_POINT ( 'NONE',  ( -88.55620429048337883, -24.64965694238574656, 8.947790433994196491 ) ) ;
#16854=EDGE_LOOP ( 'NONE', ( #45320, #71936, #76537, #79815 ) ) ;
#16855=ORIENTED_EDGE ( 'NONE', *, *, #24341, .T. ) ;
#16856=CARTESIAN_POINT ( 'NONE',  ( -111.2942365085818039, -25.18155215388633650, 3.200086650108997510 ) ) ;
#16858=CARTESIAN_POINT ( 'NONE',  ( -96.62287095715004170, -24.65952944569304606, 1.056160979905703456 ) ) ;
#16859=CARTESIAN_POINT ( 'NONE',  ( 0.1934390699377774303, 20.68474938276070318, -1.500000000000002220 ) ) ;
#16860=CARTESIAN_POINT ( 'NONE',  ( 21.43499300031224664, 3.042053824063517542, 11.49999999999999645 ) ) ;
#16861=VERTEX_POINT ( 'NONE', #67141 ) ;
#16863=CARTESIAN_POINT ( 'NONE',  ( -29.62287095715004881, -24.58390616985635546, 1.056161279468100123 ) ) ;
#16864=CARTESIAN_POINT ( 'NONE',  ( 0.3464652362752086434, -22.36268665536068667, 11.49999999999998934 ) ) ;
#16865=CARTESIAN_POINT ( 'NONE',  ( -71.52287095715011844, -24.51283580621365132, 0.6167428607019708187 ) ) ;
#16866=CARTESIAN_POINT ( 'NONE',  ( -84.54196537793758637, -24.65952944569303895, 1.056160979905700348 ) ) ;
#16867=ORIENTED_EDGE ( 'NONE', *, *, #77071, .T. ) ;
#16868=CARTESIAN_POINT ( 'NONE',  ( -100.6181544063395989, -25.31264993464104407, 4.735175672904627930 ) ) ;
#16869=CARTESIAN_POINT ( 'NONE',  ( -114.5228709571500616, -23.48786465467241769, 11.44779295918253936 ) ) ;
#16870=ORIENTED_EDGE ( 'NONE', *, *, #11842, .F. ) ;
#16871=VERTEX_POINT ( 'NONE', #45286 ) ;
#16873=EDGE_LOOP ( 'NONE', ( #90493, #85537, #93415, #67067 ) ) ;
#16874=FACE_OUTER_BOUND ( 'NONE', #28540, .T. ) ;
#16876=CARTESIAN_POINT ( 'NONE',  ( 16.87399902462237478, -12.92443306546820736, -1.500000000000002220 ) ) ;
#16878=CARTESIAN_POINT ( 'NONE',  ( -50.57412005914952147, -25.00158670708910691, 2.256160236439223254 ) ) ;
#16880=CARTESIAN_POINT ( 'NONE',  ( -18.37375256118794553, 11.78967355450649457, 11.49999999999998934 ) ) ;
#16881=CARTESIAN_POINT ( 'NONE',  ( -121.5228709571501327, -23.96177878511310055, 10.65340807706329329 ) ) ;
#16882=EDGE_CURVE ( 'NONE', #18030, #66032, #33051, .T. ) ;
#16884=CARTESIAN_POINT ( 'NONE',  ( -35.52287095715008292, -24.62285846331435835, 9.038163153548291362 ) ) ;
#16885=CARTESIAN_POINT ( 'NONE',  ( -17.41291239988371231, 13.16847401419012975, -1.500000000000002220 ) ) ;
#16886=CARTESIAN_POINT ( 'NONE',  ( -30.57287095715006231, -25.26563519389461732, 3.872667977566617292 ) ) ;
#16887=ORIENTED_EDGE ( 'NONE', *, *, #41062, .T. ) ;
#16888=CARTESIAN_POINT ( 'NONE',  ( -28.52287095715005805, -29.50250473134420659, 10.00399446418115268 ) ) ;
#16889=CARTESIAN_POINT ( 'NONE',  ( -85.59572655174477518, -24.15602025860895807, 10.28564288303535967 ) ) ;
#16890=ORIENTED_EDGE ( 'NONE', *, *, #9814, .F. ) ;
#16893=EDGE_CURVE ( 'NONE', #68291, #92642, #42769, .T. ) ;
#16894=EDGE_LOOP ( 'NONE', ( #82044, #39666, #17532, #61830 ) ) ;
#16897=CARTESIAN_POINT ( 'NONE',  ( -29.10153610609932073, -25.09928765295969910, 3.502460545500531541 ) ) ;
#16899=CARTESIAN_POINT ( 'NONE',  ( 20.00388196354723291, 7.160935007556333609, -1.500000000000002220 ) ) ;
#16900=CARTESIAN_POINT ( 'NONE',  ( -66.52287095715006160, -24.65952944569304606, 1.056160979905697239 ) ) ;
#16901=CARTESIAN_POINT ( 'NONE',  ( -130.5728709571500588, -24.36247485673955637, 0.01136689895587465055 ) ) ;
#16903=DIRECTION ( 'NONE',  ( 0.000000000000000000, -2.173523156925979552E-06, 0.9999999999976378895 ) ) ;
#16904=CARTESIAN_POINT ( 'NONE',  ( -41.52287095715005449, -23.48783264083359867, -1.443836473376375329 ) ) ;
#16905=CARTESIAN_POINT ( 'NONE',  ( 16.99290379607386114, -9.356058476803225332, -1.500000000000002220 ) ) ;
#16906=CARTESIAN_POINT ( 'NONE',  ( -117.5535883732406290, -24.35071581493544457, 9.817618358456019934 ) ) ;
#16907=VERTEX_POINT ( 'NONE', #70115 ) ;
#16908=CARTESIAN_POINT ( 'NONE',  ( -4.154358412494840280, 19.03220294597612039, 11.49999999999999645 ) ) ;
#16911=EDGE_CURVE ( 'NONE', #30482, #77370, #66848, .T. ) ;
#16912=VERTEX_POINT ( 'NONE', #47788 ) ;
#16913=AXIS2_PLACEMENT_3D ( 'NONE', #12106, #82620, #27840 ) ;
#16915=CARTESIAN_POINT ( 'NONE',  ( -128.5228709571500758, -29.50250786944525672, 11.44777988621622633 ) ) ;
#16916=CARTESIAN_POINT ( 'NONE',  ( -91.62287095715005592, -23.72773821059536559, 11.05748984161097503 ) ) ;
#16918=CARTESIAN_POINT ( 'NONE',  ( -19.15055961920884542, -4.482958728538418924, 11.49999999999998934 ) ) ;
#16919=EDGE_CURVE ( 'NONE', #23684, #44074, #1108, .T. ) ;
#16920=EDGE_LOOP ( 'NONE', ( #48596, #44479, #41159, #39484, #84430, #9317, #53112, #57188, #14147, #76016 ) ) ;
#16921=CARTESIAN_POINT ( 'NONE',  ( -7.206546067468990735, 20.34698395366585189, -1.500000000000002220 ) ) ;
#16923=CARTESIAN_POINT ( 'NONE',  ( -90.52287095715001897, -23.85229601348996908, 10.88205029486208275 ) ) ;
#16924=CARTESIAN_POINT ( 'NONE',  ( 1.767912858038628965, -23.04938964843747584, -1.500000000000002220 ) ) ;
#16926=CARTESIAN_POINT ( 'NONE',  ( -38.52287095715006870, -29.50248528299804818, 1.056150453629031594 ) ) ;
#16927=CARTESIAN_POINT ( 'NONE',  ( -105.6228709571500559, -23.47596703998600631, 11.44779298504227860 ) ) ;
#16928=CARTESIAN_POINT ( 'NONE',  ( -84.62287095715005592, -24.64965695001469115, 8.947790433994182280 ) ) ;
#16929=CARTESIAN_POINT ( 'NONE',  ( -104.5228709571500758, -24.50321055353806088, 9.387540953477520489 ) ) ;
#16931=CARTESIAN_POINT ( 'NONE',  ( -124.5228709571500616, -23.48786465467241769, 11.44779295918253759 ) ) ;
#16932=CARTESIAN_POINT ( 'NONE',  ( -114.5542467394807318, -24.15620529776629510, 10.23563542870659404 ) ) ;
#16933=CARTESIAN_POINT ( 'NONE',  ( 7.348632388941331861, 18.53259892055224611, 11.49999999999998934 ) ) ;
#16935=CARTESIAN_POINT ( 'NONE',  ( -100.9404532381483079, -25.21193246312661529, 3.416343243334487578 ) ) ;
#16936=CARTESIAN_POINT ( 'NONE',  ( -14.51517298184297289, -13.48802281452852725, -1.500000000000002220 ) ) ;
#16943=CARTESIAN_POINT ( 'NONE',  ( 12.20387445076365296, 16.77033177596414504, 11.49999999999999645 ) ) ;
#16944=CARTESIAN_POINT ( 'NONE',  ( -70.74026866089612042, -29.50249362659879537, 4.894895270847094970 ) ) ;
#16945=B_SPLINE_CURVE_WITH_KNOTS ( 'NONE', 3,
 ( #69492, #85713, #100409, #47160 ),
 .UNSPECIFIED., .F., .F.,
 ( 4, 4 ),
 ( 0.000000000000000000, 0.002769230769230773825 ),
 .UNSPECIFIED. ) ;
#16947=LINE ( 'NONE', #1236, #2031 ) ;
#16948=CARTESIAN_POINT ( 'NONE',  ( 10.97283692364161922, -19.94330716608196852, 11.49999999999999645 ) ) ;
#16949=EDGE_LOOP ( 'NONE', ( #87156, #10976, #72796, #72024 ) ) ;
#16950=CARTESIAN_POINT ( 'NONE',  ( -112.2228709571500502, -23.47596703998600631, 11.44779298504227860 ) ) ;
#16951=CARTESIAN_POINT ( 'NONE',  ( -38.52287095715008292, -23.48783264083452593, -1.443836473374935592 ) ) ;
#16952=ORIENTED_EDGE ( 'NONE', *, *, #84929, .T. ) ;
#16953=CARTESIAN_POINT ( 'NONE',  ( -19.21899500656021331, -6.280627263257740900, -1.500000000000002220 ) ) ;
#16955=CARTESIAN_POINT ( 'NONE',  ( -67.62287095715005592, -29.50250243563736774, 8.947779886222143375 ) ) ;
#16957=CARTESIAN_POINT ( 'NONE',  ( -32.62287095715004881, -23.48783264082477729, -1.443836473390074371 ) ) ;
#16958=CARTESIAN_POINT ( 'NONE',  ( -17.89994474767736676, -14.32179853049041363, 11.49999999999998934 ) ) ;
#16959=CARTESIAN_POINT ( 'NONE',  ( -84.52287095715003318, -24.33927499327855060, 9.819080762295811837 ) ) ;
#16960=CARTESIAN_POINT ( 'NONE',  ( -18.81269933604069067, 6.858547123926768130, -1.500000000000002220 ) ) ;
#16961=CARTESIAN_POINT ( 'NONE',  ( -36.62287095715007723, -23.95044443724991368, 10.65354141964650125 ) ) ;
#16962=CARTESIAN_POINT ( 'NONE',  ( -15.18370147500227496, -14.46048895944246127, 11.49999999999999645 ) ) ;
#16963=CARTESIAN_POINT ( 'NONE',  ( -59.56094173781918499, -25.21083105912962097, 3.409327675794633805 ) ) ;
#16964=CARTESIAN_POINT ( 'NONE',  ( -68.99199226862026535, -25.24754449216967345, 5.787353197655024317 ) ) ;
#16965=CARTESIAN_POINT ( 'NONE',  ( 17.21905055353458991, -13.78536315820828229, 11.49999999999998934 ) ) ;
#16973=ORIENTED_EDGE ( 'NONE', *, *, #42594, .F. ) ;
#16975=CARTESIAN_POINT ( 'NONE',  ( -101.6430330839730516, -25.26303730729093999, 3.986250639247583827 ) ) ;
#16976=CARTESIAN_POINT ( 'NONE',  ( -80.62287095715004170, -23.48786465467241058, 11.44779295918254469 ) ) ;
#16977=CARTESIAN_POINT ( 'NONE',  ( -100.5228709571500616, -24.99156044556120904, 7.747789690856173195 ) ) ;
#16978=CARTESIAN_POINT ( 'NONE',  ( -16.44861368136865920, 12.28130381464353782, -1.500000000000002220 ) ) ;
#16981=CARTESIAN_POINT ( 'NONE',  ( -105.6228709571500559, -29.50250786944525672, 11.44777988621622988 ) ) ;
#16982=CARTESIAN_POINT ( 'NONE',  ( -44.58708426901613819, -24.34968618360933235, 0.1864209137778787551 ) ) ;
#16983=DIRECTION ( 'NONE',  ( -3.773278334453079618E-23, 0.9999999999976377785, 2.173523156925979975E-06 ) ) ;
#16984=CARTESIAN_POINT ( 'NONE',  ( -10.38793682863964563, 19.71736701935523683, -1.500000000000002220 ) ) ;
#16985=CARTESIAN_POINT ( 'NONE',  ( -55.52287095715007581, -23.85229601348996198, 10.88205029486209519 ) ) ;
#16987=EDGE_LOOP ( 'NONE', ( #17529, #50107, #32995, #72050 ) ) ;
#16988=CARTESIAN_POINT ( 'NONE',  ( -47.62287095715004881, -29.50250786944525672, 11.44777988621624054 ) ) ;
#16989=CARTESIAN_POINT ( 'NONE',  ( -118.5228709571500474, -23.94994826722564696, -0.6494450866342723616 ) ) ;
#16990=CARTESIAN_POINT ( 'NONE',  ( 8.324980675869593227, 19.10421180063631752, -1.500000000000002220 ) ) ;
#16992=CARTESIAN_POINT ( 'NONE',  ( -52.52287095715006870, -29.50250243563736774, 8.947779886222146928 ) ) ;
#16993=VERTEX_POINT ( 'NONE', #77706 ) ;
#16996=CARTESIAN_POINT ( 'NONE',  ( -103.9228709571500673, -23.47593901973090169, -1.443836447538996648 ) ) ;
#16997=CARTESIAN_POINT ( 'NONE',  ( -17.07941033872765146, 12.18221932706078370, -1.500000000000002220 ) ) ;
#16998=VERTEX_POINT ( 'NONE', #63022 ) ;
#17002=CARTESIAN_POINT ( 'NONE',  ( -95.52287095715006160, -23.48786465467241769, 11.44779295918254114 ) ) ;
#17003=B_SPLINE_CURVE_WITH_KNOTS ( 'NONE', 3,
 ( #31746, #68314, #45489, #37862 ),
 .UNSPECIFIED., .F., .F.,
 ( 4, 4 ),
 ( 0.000000000000000000, 1.000000000000000000 ),
 .UNSPECIFIED. ) ;
#17004=CARTESIAN_POINT ( 'NONE',  ( -100.9913061220214843, -25.25419536262793230, 7.480517119236268719 ) ) ;
#17005=CARTESIAN_POINT ( 'NONE',  ( -59.55981030432491963, -23.73766607897669445, -1.055555164236460675 ) ) ;
#17007=CARTESIAN_POINT ( 'NONE',  ( -65.62287095715009855, -24.15516710230293995, 10.28746687063726029 ) ) ;
#17008=CARTESIAN_POINT ( 'NONE',  ( 10.53326394202159300, -19.55463526559320542, 11.49999999999999645 ) ) ;
#17011=CARTESIAN_POINT ( 'NONE',  ( -71.25851563654804011, -25.27180963933369284, 5.909805672228780615 ) ) ;
#17012=ORIENTED_EDGE ( 'NONE', *, *, #9653, .F. ) ;
#17013=EDGE_CURVE ( 'NONE', #11637, #14276, #68091, .T. ) ;
#17014=CARTESIAN_POINT ( 'NONE',  ( -15.33504971967173702, 16.71734053393862496, -1.500000000000002220 ) ) ;
#17018=ADVANCED_FACE ( 'NONE', ( #69105 ), #62510, .F. ) ;
#17021=ADVANCED_FACE ( 'NONE', ( #23932 ), #3743, .T. ) ;
#17023=CARTESIAN_POINT ( 'NONE',  ( -6.497366621441947210, -19.08602653180391329, 11.49999999999998934 ) ) ;
#17024=CARTESIAN_POINT ( 'NONE',  ( -99.55620429048339304, -23.47596703998600631, 11.44779298504227683 ) ) ;
#17026=CARTESIAN_POINT ( 'NONE',  ( -58.62287095715004881, -23.48783264082478439, -1.443836473390069264 ) ) ;
#17027=CARTESIAN_POINT ( 'NONE',  ( 18.65981798208652265, 12.38953945867474360, -1.500000000000002220 ) ) ;
#17028=VERTEX_POINT ( 'NONE', #2122 ) ;
#17029=VERTEX_POINT ( 'NONE', #72632 ) ;
#17030=CARTESIAN_POINT ( 'NONE',  ( -112.6270362718817779, -24.15620529776628445, 10.23563542870659582 ) ) ;
#17031=CARTESIAN_POINT ( 'NONE',  ( -94.51552167049113962, -23.96169478059713143, 10.65365249895717881 ) ) ;
#17034=DIRECTION ( 'NONE',  ( -3.773278334453080206E-23, 0.9999999999976377785, 2.173523156925979975E-06 ) ) ;
#17035=CARTESIAN_POINT ( 'NONE',  ( -4.924063254364682507, -18.92933890202812464, 11.49999999999998934 ) ) ;
#17036=B_SPLINE_CURVE_WITH_KNOTS ( 'NONE', 3,
 ( #31503, #61472, #99992, #92395 ),
 .UNSPECIFIED., .F., .F.,
 ( 4, 4 ),
 ( 0.000000000000000000, 9.999999999997510880E-05 ),
 .UNSPECIFIED. ) ;
#17039=CARTESIAN_POINT ( 'NONE',  ( -2.374466145016132845, -21.38244973876172494, 11.49999999999998934 ) ) ;
#17040=CARTESIAN_POINT ( 'NONE',  ( -36.52287095715006870, -24.51283580621364777, 0.6167428607019721509 ) ) ;
#17041=CARTESIAN_POINT ( 'NONE',  ( -54.62287095715006302, -23.72773821059535493, 11.05748984161097503 ) ) ;
#17044=CARTESIAN_POINT ( 'NONE',  ( 21.91704834537361180, 6.644925864936762849, -1.500000000000002220 ) ) ;
#17047=CARTESIAN_POINT ( 'NONE',  ( -85.22287095715007865, -23.47596703998600631, 11.44779298504227860 ) ) ;
#17048=CARTESIAN_POINT ( 'NONE',  ( -53.51456551345987123, -23.73766607897669800, -1.055555164236460008 ) ) ;
#17049=CARTESIAN_POINT ( 'NONE',  ( 11.39338536883839659, -16.50304575528446804, 11.49999999999999645 ) ) ;
#17050=CARTESIAN_POINT ( 'NONE',  ( -80.35919894935766195, -25.26612373672872636, 4.505481401771154637 ) ) ;
#17052=CARTESIAN_POINT ( 'NONE',  ( -73.52287095715010423, -23.48783264082477018, -1.443836473390093689 ) ) ;
#17053=LINE ( 'NONE', #56642, #42391 ) ;
#17054=CARTESIAN_POINT ( 'NONE',  ( -118.6228709571500701, -23.48783264082478794, -1.443836473390058384 ) ) ;
#17055=VECTOR ( 'NONE', #3432, 1000.000000000000114 ) ;
#17056=CARTESIAN_POINT ( 'NONE',  ( -4.706806674773570620, -21.25045708977441450, 11.49999999999998934 ) ) ;
#17058=CARTESIAN_POINT ( 'NONE',  ( -6.723608784814384620, 18.44229941887336821, -1.500000000000002220 ) ) ;
#17061=CARTESIAN_POINT ( 'NONE',  ( -110.2093792378191921, -25.31698244681350474, 5.585409175846506535 ) ) ;
#17063=FACE_OUTER_BOUND ( 'NONE', #26514, .T. ) ;
#17064=CARTESIAN_POINT ( 'NONE',  ( -98.62287095715005592, -24.66019654487199730, 8.947790411086124607 ) ) ;
#17065=CARTESIAN_POINT ( 'NONE',  ( 13.18781518674367348, -15.76626393773247337, 11.49999999999999645 ) ) ;
#17067=ADVANCED_FACE ( 'NONE', ( #57911 ), #88855, .T. ) ;
#17068=CARTESIAN_POINT ( 'NONE',  ( -120.5553418306319884, -24.15503026093913874, -0.2815557561904507011 ) ) ;
#17069=CARTESIAN_POINT ( 'NONE',  ( 8.141615846073909424, -21.09679883994429161, 11.49999999999999645 ) ) ;
#17071=ADVANCED_FACE ( 'NONE', ( #79720 ), #95450, .T. ) ;
#17072=CARTESIAN_POINT ( 'NONE',  ( -100.6258216950799778, -25.31296450549008625, 4.735305783089845733 ) ) ;
#17074=CARTESIAN_POINT ( 'NONE',  ( -125.5894637005920629, -24.63419186844610920, 9.035850630976920428 ) ) ;
#17075=CARTESIAN_POINT ( 'NONE',  ( -27.12628703559276389, -24.76673041788330920, 2.399896000618569669 ) ) ;
#17076=B_SPLINE_CURVE_WITH_KNOTS ( 'NONE', 3,
 ( #77295, #4449, #38241, #38741, #74925, #5429 ),
 .UNSPECIFIED., .F., .F.,
 ( 4, 2, 4 ),
 ( 0.000000000000000000, 0.001380901958385391580, 0.002761803916770783161 ),
 .UNSPECIFIED. ) ;
#17078=CARTESIAN_POINT ( 'NONE',  ( -127.5228709571500616, -29.50250786944525672, 11.44777988621622633 ) ) ;
#17079=B_SPLINE_CURVE_WITH_KNOTS ( 'NONE', 3,
 ( #83966, #85456, #14945, #45917, #15445, #93562 ),
 .UNSPECIFIED., .F., .F.,
 ( 4, 2, 4 ),
 ( 1.570887131794952276E-05, 0.001396322306279764325, 0.002776935741241578874 ),
 .UNSPECIFIED. ) ;
#17081=CARTESIAN_POINT ( 'NONE',  ( -80.19887417545862718, -25.31596225461789729, 4.982290565433718399 ) ) ;
#17082=CARTESIAN_POINT ( 'NONE',  ( 7.824713763024562674, 21.46283361357968289, -1.500000000000002220 ) ) ;
#17083=CARTESIAN_POINT ( 'NONE',  ( 5.514125806255895004E-17, -29.50250243563707286, 8.947779751028683393 ) ) ;
#17084=CARTESIAN_POINT ( 'NONE',  ( -72.55620429048340725, -24.66019654487199020, 8.947790411086131712 ) ) ;
#17085=CARTESIAN_POINT ( 'NONE',  ( -82.58247480767941795, -24.66019654487199730, 8.947790411086122830 ) ) ;
#17086=AXIS2_PLACEMENT_3D ( 'NONE', #86214, #84204, #71000 ) ;
#17087=CARTESIAN_POINT ( 'NONE',  ( 6.846561153812083411, -21.39451737393737574, 11.49999999999999645 ) ) ;
#17089=CARTESIAN_POINT ( 'NONE',  ( -81.62287095715005592, -29.50250786944525672, 11.44777988621623521 ) ) ;
#17090=CARTESIAN_POINT ( 'NONE',  ( -8.017166757594178961, 20.41873492177044724, -1.500000000000002220 ) ) ;
#17092=ADVANCED_FACE ( 'NONE', ( #65038 ), #73127, .F. ) ;
#17093=CARTESIAN_POINT ( 'NONE',  ( -114.5228709571500758, -24.33927499327856125, 9.819080762295810061 ) ) ;
#17094=CARTESIAN_POINT ( 'NONE',  ( -34.59402351810827980, -24.15620529776627379, 10.23563542870661003 ) ) ;
#17095=DIRECTION ( 'NONE',  ( -3.773278334453079618E-23, 0.9999999999976377785, 2.173523156925979975E-06 ) ) ;
#17096=EDGE_LOOP ( 'NONE', ( #59932, #23722, #25104, #43084 ) ) ;
#17097=CARTESIAN_POINT ( 'NONE',  ( -48.66106295358616052, -23.48786465467241058, 11.44779295918254824 ) ) ;
#17098=DIRECTION ( 'NONE',  ( 3.773278334444167608E-23, -1.000000000000000000, 0.000000000000000000 ) ) ;
#17099=EDGE_LOOP ( 'NONE', ( #8402, #77414, #54285, #7545 ) ) ;
#17100=CARTESIAN_POINT ( 'NONE',  ( -19.64171699416042571, -5.764624264842452384, 11.49999999999998934 ) ) ;
#17101=VERTEX_POINT ( 'NONE', #63523 ) ;
#17103=EDGE_LOOP ( 'NONE', ( #2315, #89100, #71167, #66441 ) ) ;
#17105=CARTESIAN_POINT ( 'NONE',  ( 19.40787663092975279, -12.54570180764831377, -1.500000000000002220 ) ) ;
#17106=CARTESIAN_POINT ( 'NONE',  ( -40.79597241634589722, -25.30977039686255026, 4.487062071701387822 ) ) ;
#17107=CARTESIAN_POINT ( 'NONE',  ( 16.59675031405745571, -11.69241480613374407, -1.500000000000002220 ) ) ;
#17109=PLANE ( 'NONE',  #7195 ) ;
#17110=CARTESIAN_POINT ( 'NONE',  ( -72.52287095715009002, -23.72747288104470087, -1.053458166803226570 ) ) ;
#17111=DIRECTION ( 'NONE',  ( -1.000000000000000000, -3.773278334444167608E-23, -8.201307833595939069E-29 ) ) ;
#17113=CARTESIAN_POINT ( 'NONE',  ( -16.68621059303058018, 13.52761613308161870, 11.49999999999999645 ) ) ;
#17114=ORIENTED_EDGE ( 'NONE', *, *, #60800, .F. ) ;
#17115=FACE_OUTER_BOUND ( 'NONE', #8373, .T. ) ;
#17118=CARTESIAN_POINT ( 'NONE',  ( 14.12806351585482112, -15.20395780304818523, 11.49999999999998934 ) ) ;
#17123=CARTESIAN_POINT ( 'NONE',  ( -75.62287095715004170, -24.99156045073392818, 7.747789690856161648 ) ) ;
#17124=CARTESIAN_POINT ( 'NONE',  ( -53.52287095715008292, -23.48783264082477018, -1.443836473390094799 ) ) ;
#17128=CARTESIAN_POINT ( 'NONE',  ( -42.53413042267195010, -24.51419770103158413, 9.386484678747191168 ) ) ;
#17130=CARTESIAN_POINT ( 'NONE',  ( -43.63415880193262097, -24.35071581493542325, 9.817618358456034144 ) ) ;
#17131=CARTESIAN_POINT ( 'NONE',  ( -1.213202359833694732, 22.00568734548514627, 11.49999999999999645 ) ) ;
#17132=ORIENTED_EDGE ( 'NONE', *, *, #38960, .F. ) ;
#17133=AXIS2_PLACEMENT_3D ( 'NONE', #84098, #14583, #6980 ) ;
#17134=CARTESIAN_POINT ( 'NONE',  ( -103.5953259629072392, -23.73766607897670156, -1.055555164236454901 ) ) ;
#17136=CARTESIAN_POINT ( 'NONE',  ( -12.77507031947300042, 18.62636059118606724, 11.49999999999998934 ) ) ;
#17137=VECTOR ( 'NONE', #22444, 1000.000000000000114 ) ;
#17138=CARTESIAN_POINT ( 'NONE',  ( 3.785439364192078937, -20.66625369722972749, -1.500000000000002220 ) ) ;
#17139=LINE ( 'NONE', #10528, #13405 ) ;
#17140=VERTEX_POINT ( 'NONE', #9207 ) ;
#17141=EDGE_CURVE ( 'NONE', #81135, #75736, #89832, .T. ) ;
#17147=CARTESIAN_POINT ( 'NONE',  ( 20.71511372717374755, 4.256074106246791722, -1.500000000000002220 ) ) ;
#17149=CARTESIAN_POINT ( 'NONE',  ( -51.90898564286461436, -25.26040870674269101, 6.429377479227253112 ) ) ;
#17150=CARTESIAN_POINT ( 'NONE',  ( -88.62287095714998486, -24.33927499327853994, 9.819080762295810061 ) ) ;
#17151=CARTESIAN_POINT ( 'NONE',  ( -28.62287095715004881, -23.33150569529546914, 11.44779297407613150 ) ) ;
#17153=CARTESIAN_POINT ( 'NONE',  ( -19.03210976516136554, 11.49075778266564107, -1.500000000000002220 ) ) ;
#17154=CARTESIAN_POINT ( 'NONE',  ( -114.5222273449358141, -23.48783264082478794, -1.443836473390062380 ) ) ;
#17155=EDGE_CURVE ( 'NONE', #73714, #13179, #71624, .T. ) ;
#17156=ORIENTED_EDGE ( 'NONE', *, *, #32616, .F. ) ;
#17158=CARTESIAN_POINT ( 'NONE',  ( -37.63490762544056167, -24.34968618360933590, 0.1864209137778856384 ) ) ;
#17159=CARTESIAN_POINT ( 'NONE',  ( -126.6239571621962341, -24.34968618360934300, 0.1864209137778884418 ) ) ;
#17160=CARTESIAN_POINT ( 'NONE',  ( -100.5858031092710547, -24.83618233451450763, 1.606449574219537713 ) ) ;
#17162=CARTESIAN_POINT ( 'NONE',  ( 1.793504005174451077, 19.40006364325761012, 11.49999999999998934 ) ) ;
#17163=B_SPLINE_CURVE_WITH_KNOTS ( 'NONE', 3,
 ( #45700, #7126, #38582, #44206, #69541, #38076 ),
 .UNSPECIFIED., .F., .F.,
 ( 4, 2, 4 ),
 ( 0.000000000000000000, 0.001380901958385383774, 0.002761803916770767548 ),
 .UNSPECIFIED. ) ;
#17164=CARTESIAN_POINT ( 'NONE',  ( -19.74196057798672399, -8.316236533413031040, 11.49999999999998934 ) ) ;
#17166=CARTESIAN_POINT ( 'NONE',  ( -60.62821527951275868, -24.83644354574317603, 8.397322867105112110 ) ) ;
#17167=CARTESIAN_POINT ( 'NONE',  ( -113.5228709571500616, -29.50250243563736774, 8.947779886222136270 ) ) ;
#17168=CARTESIAN_POINT ( 'NONE',  ( -36.62287095715005592, -23.47593901973091235, -1.443836447539011525 ) ) ;
#17169=CARTESIAN_POINT ( 'NONE',  ( 2.720868037236281012, -22.60253418658637869, -1.500000000000002220 ) ) ;
#17171=CARTESIAN_POINT ( 'NONE',  ( -98.62287095715004170, -24.65952944569304606, 1.056160979905700792 ) ) ;
#17172=CARTESIAN_POINT ( 'NONE',  ( -4.768723929037996356, 19.30091236029735668, 11.49999999999999645 ) ) ;
#17174=CARTESIAN_POINT ( 'NONE',  ( -108.5895376238167245, -23.48786465467242479, 11.44779295918253759 ) ) ;
#17175=LINE ( 'NONE', #56767, #87780 ) ;
#17176=VERTEX_POINT ( 'NONE', #51280 ) ;
#17180=CARTESIAN_POINT ( 'NONE',  ( -18.79206335510377102, -10.79472360063173397, -1.500000000000002220 ) ) ;
#17182=CARTESIAN_POINT ( 'NONE',  ( -16.97169330436246781, 9.548981535075045102, -1.500000000000002220 ) ) ;
#17184=CARTESIAN_POINT ( 'NONE',  ( -55.58900237498185959, -24.52399227489126687, 9.353111116836526406 ) ) ;
#17187=CARTESIAN_POINT ( 'NONE',  ( 5.143668500415711442, -19.74887971880038151, 11.49999999999999645 ) ) ;
#17189=EDGE_CURVE ( 'NONE', #10158, #70435, #5600, .T. ) ;
#17190=VECTOR ( 'NONE', #83474, 1000.000000000000114 ) ;
#17191=DIRECTION ( 'NONE',  ( 1.000000000000000000, 3.773278334444167608E-23, 8.201307833595939069E-29 ) ) ;
#17192=VERTEX_POINT ( 'NONE', #27943 ) ;
#17194=CARTESIAN_POINT ( 'NONE',  ( -39.14714599385568761, -25.31628570854560678, 4.777938624344938212 ) ) ;
#17195=VECTOR ( 'NONE', #62325, 1000.000000000000114 ) ;
#17198=CARTESIAN_POINT ( 'NONE',  ( -74.52287095715007581, -29.50248528299804818, 1.056150453629036701 ) ) ;
#17199=CARTESIAN_POINT ( 'NONE',  ( 19.99232773509726258, 2.034096180923423702, -1.500000000000002220 ) ) ;
#17202=ORIENTED_EDGE ( 'NONE', *, *, #31718, .F. ) ;
#17203=CARTESIAN_POINT ( 'NONE',  ( -66.58774706379415420, -24.35071581493543036, 9.817618358456028815 ) ) ;
#17205=CARTESIAN_POINT ( 'NONE',  ( 8.986065527603487979, -21.13286776747340667, 11.49999999999999645 ) ) ;
#17206=CARTESIAN_POINT ( 'NONE',  ( 21.04450177026006230, 8.645109164175620364, -1.500000000000002220 ) ) ;
#17207=ORIENTED_EDGE ( 'NONE', *, *, #2457, .F. ) ;
#17208=CARTESIAN_POINT ( 'NONE',  ( -45.52287095715007581, -24.83602698348159876, 1.605859176311259295 ) ) ;
#17211=CARTESIAN_POINT ( 'NONE',  ( -30.57287095715005876, -24.49485400407631985, 0.5870690654870184266 ) ) ;
#17214=CARTESIAN_POINT ( 'NONE',  ( -26.09825057249113556, -24.95872903603973469, 4.796238057267346200 ) ) ;
#17215=CARTESIAN_POINT ( 'NONE',  ( -90.58953762381672448, -23.48783264082478794, -1.443836473390063713 ) ) ;
#17216=CARTESIAN_POINT ( 'NONE',  ( -58.64946100639908622, -23.73766607897669800, -1.055555164236457344 ) ) ;
#17218=CARTESIAN_POINT ( 'NONE',  ( -2.125485521908593078, 20.27274140177646444, -1.500000000000002220 ) ) ;
#17220=VERTEX_POINT ( 'NONE', #89347 ) ;
#17221=CARTESIAN_POINT ( 'NONE',  ( -22.63010559926462051, 4.001702944626347680, 11.49999999999998934 ) ) ;
#17224=ORIENTED_EDGE ( 'NONE', *, *, #25982, .F. ) ;
#17226=CARTESIAN_POINT ( 'NONE',  ( -108.5222109042165357, -23.48786465467241413, 11.44779295918253759 ) ) ;
#17228=CARTESIAN_POINT ( 'NONE',  ( -98.62287095715005592, -24.66019654487199730, 8.947790411086124607 ) ) ;
#17229=CARTESIAN_POINT ( 'NONE',  ( -119.2834334325141583, -25.28353533326600555, 5.756556888876060540 ) ) ;
#17230=CARTESIAN_POINT ( 'NONE',  ( 10.72677997844354536, -18.41129465587203740, 11.49999999999999645 ) ) ;
#17231=ORIENTED_EDGE ( 'NONE', *, *, #41195, .F. ) ;
#17232=ORIENTED_EDGE ( 'NONE', *, *, #50651, .F. ) ;
#17233=CARTESIAN_POINT ( 'NONE',  ( -21.14947813473477822, 6.846651710974520633, -1.500000000000002220 ) ) ;
#17234=CARTESIAN_POINT ( 'NONE',  ( 7.614520588612671226, -19.20288753073135268, 11.49999999999998934 ) ) ;
#17235=B_SPLINE_CURVE_WITH_KNOTS ( 'NONE', 3,
 ( #4066, #68334, #42145, #88304 ),
 .UNSPECIFIED., .F., .F.,
 ( 4, 4 ),
 ( 0.000000000000000000, 1.000000000000000000 ),
 .UNSPECIFIED. ) ;
#17237=DIRECTION ( 'NONE',  ( -3.773278334444166432E-23, 1.000000000000000000, 0.000000000000000000 ) ) ;
#17238=CARTESIAN_POINT ( 'NONE',  ( -95.59105585138695460, -24.40133493613050319, 9.663955038902802386 ) ) ;
#17240=CARTESIAN_POINT ( 'NONE',  ( -127.6228709571500559, -24.64898659630368627, 1.056161002820834804 ) ) ;
#17241=ORIENTED_EDGE ( 'NONE', *, *, #44990, .T. ) ;
#17242=CARTESIAN_POINT ( 'NONE',  ( -58.62774179497608174, -24.51419770103156637, 9.386484678747176957 ) ) ;
#17243=CARTESIAN_POINT ( 'NONE',  ( -71.09456214124740825, -25.17613501044473878, 6.773754074536313396 ) ) ;
#17244=CARTESIAN_POINT ( 'NONE',  ( -19.40664508603899563, 7.695215611089875729, -1.500000000000002220 ) ) ;
#17246=CARTESIAN_POINT ( 'NONE',  ( -0.06377455873143267340, 21.83884041771831619, 11.49999999999999645 ) ) ;
#17247=CARTESIAN_POINT ( 'NONE',  ( -89.81226385320383088, -25.22391155068715207, 6.409327647370969494 ) ) ;
#17249=CARTESIAN_POINT ( 'NONE',  ( -17.89120377161202313, 13.61666483413312712, 11.49999999999998934 ) ) ;
#17251=CARTESIAN_POINT ( 'NONE',  ( -118.6277898053671578, -23.73791477778912551, 11.05961554403169878 ) ) ;
#17253=CARTESIAN_POINT ( 'NONE',  ( -59.58953762381674579, -23.47596703998600276, 11.44779298504227505 ) ) ;
#17254=ORIENTED_EDGE ( 'NONE', *, *, #81840, .F. ) ;
#17255=EDGE_CURVE ( 'NONE', #28117, #47607, #87306, .T. ) ;
#17256=ORIENTED_EDGE ( 'NONE', *, *, #56419, .F. ) ;
#17260=EDGE_LOOP ( 'NONE', ( #89250, #30683, #96846, #93485 ) ) ;
#17262=CARTESIAN_POINT ( 'NONE',  ( -7.526967427842778946, 20.06989004931119425, -1.500000000000002220 ) ) ;
#17263=CARTESIAN_POINT ( 'NONE',  ( 8.681249458320607459, -20.60847208623538762, 11.49999999999999645 ) ) ;
#17266=AXIS2_PLACEMENT_3D ( 'NONE', #82506, #12990, #43953 ) ;
#17267=CARTESIAN_POINT ( 'NONE',  ( 20.75205275252385206, -3.532026382766447536, 11.49999999999998934 ) ) ;
#17268=CARTESIAN_POINT ( 'NONE',  ( -30.47815444756320602, -24.83107907226382238, 8.370654131274083198 ) ) ;
#17269=CARTESIAN_POINT ( 'NONE',  ( 7.348632388941331861, 18.53259892055224611, -1.500000000000002220 ) ) ;
#17270=CARTESIAN_POINT ( 'NONE',  ( -50.63858115698904072, -24.52399227489127043, 9.353111116836521077 ) ) ;
#17273=CARTESIAN_POINT ( 'NONE',  ( -21.42919730060085115, -5.301375089729956969, -1.500000000000002220 ) ) ;
#17274=ORIENTED_EDGE ( 'NONE', *, *, #44403, .T. ) ;
#17275=DIRECTION ( 'NONE',  ( -3.773278334453079030E-23, 0.9999999999976377785, 2.173523156925979128E-06 ) ) ;
#17277=CARTESIAN_POINT ( 'NONE',  ( -121.5228709571500900, -23.94994826722565406, -0.6494450866342689199 ) ) ;
#17278=CARTESIAN_POINT ( 'NONE',  ( -16.98601802344612111, -12.12340321765213069, 11.49999999999999645 ) ) ;
#17281=CARTESIAN_POINT ( 'NONE',  ( -129.2228709571500644, -23.47596703998600631, 11.44779298504227860 ) ) ;
#17282=CARTESIAN_POINT ( 'NONE',  ( -119.6228709571500701, -23.48786465467241769, 11.44779295918253759 ) ) ;
#17283=CARTESIAN_POINT ( 'NONE',  ( -20.14006130340733236, -7.001243683211865410, -1.500000000000002220 ) ) ;
#17284=CARTESIAN_POINT ( 'NONE',  ( -121.5228709571500616, -24.64965694238408034, 8.947790433994191162 ) ) ;
#17285=CARTESIAN_POINT ( 'NONE',  ( -51.26173465382703398, -25.25485035848373983, 3.787228214310553120 ) ) ;
#17286=CARTESIAN_POINT ( 'NONE',  ( -96.52287095715001897, -24.35013146730204525, 9.818937971375097717 ) ) ;
#17287=CARTESIAN_POINT ( 'NONE',  ( -70.65333586436670998, -25.30188801935125653, 5.302352381037461093 ) ) ;
#17288=CARTESIAN_POINT ( 'NONE',  ( -9.785633969878258398, 20.35780147342342516, -1.500000000000002220 ) ) ;
#17290=ORIENTED_EDGE ( 'NONE', *, *, #90243, .T. ) ;
#17292=CARTESIAN_POINT ( 'NONE',  ( -31.52579011953796950, -24.66019654487199020, 8.947790411086133489 ) ) ;
#17293=CARTESIAN_POINT ( 'NONE',  ( -10.66912846187372210, -16.51573522771486324, 11.49999999999999645 ) ) ;
#17296=ORIENTED_EDGE ( 'NONE', *, *, #33540, .F. ) ;
#17297=CARTESIAN_POINT ( 'NONE',  ( -111.5228709571500616, -24.64898659630368627, 1.056161002820831474 ) ) ;
#17298=CARTESIAN_POINT ( 'NONE',  ( -39.55620429048340014, -24.65952944569304606, 1.056160979905692354 ) ) ;
#17299=CARTESIAN_POINT ( 'NONE',  ( -124.6262003333403925, -23.48786465467241769, 11.44779295918253581 ) ) ;
#17300=AXIS2_PLACEMENT_3D ( 'NONE', #75757, #30589, #52443 ) ;
#17302=CARTESIAN_POINT ( 'NONE',  ( -107.5228709571500758, -24.64965694238575011, 8.947790433994192938 ) ) ;
#17303=CARTESIAN_POINT ( 'NONE',  ( 17.05426814964238957, 9.943002105365778220, -1.500000000000002220 ) ) ;
#17306=CARTESIAN_POINT ( 'NONE',  ( 19.60372117168125072, 4.849774137724135237, 11.49999999999999645 ) ) ;
#17308=EDGE_CURVE ( 'NONE', #12501, #27247, #47413, .T. ) ;
#17309=ORIENTED_EDGE ( 'NONE', *, *, #35936, .F. ) ;
#17310=FACE_OUTER_BOUND ( 'NONE', #76572, .T. ) ;
#17311=CARTESIAN_POINT ( 'NONE',  ( -65.58953762381672448, -23.48786465467241058, 11.44779295918254647 ) ) ;
#17312=LINE ( 'NONE', #34051, #65539 ) ;
#17313=FACE_OUTER_BOUND ( 'NONE', #52575, .T. ) ;
#17314=B_SPLINE_CURVE_WITH_KNOTS ( 'NONE', 3,
 ( #74957, #29293, #68364, #36410 ),
 .UNSPECIFIED., .F., .F.,
 ( 4, 4 ),
 ( 2.232523134950097154E-11, 0.0004693952269521748277 ),
 .UNSPECIFIED. ) ;
#17317=CARTESIAN_POINT ( 'NONE',  ( 11.47056939498152950, -16.38825109899074661, -1.500000000000002220 ) ) ;
#17318=B_SPLINE_CURVE_WITH_KNOTS ( 'NONE', 3,
 ( #86560, #31775, #6062, #32269 ),
 .UNSPECIFIED., .F., .F.,
 ( 4, 4 ),
 ( 1.387778780781445521E-17, 9.999999999997510880E-05 ),
 .UNSPECIFIED. ) ;
#17319=CARTESIAN_POINT ( 'NONE',  ( -117.5895376238167245, -24.64898659630368627, 1.056161002820392270 ) ) ;
#17322=VECTOR ( 'NONE', #57864, 1000.000000000000114 ) ;
#17324=CARTESIAN_POINT ( 'NONE',  ( -33.62287095715005592, -23.96127896941631619, -0.6493128931037960294 ) ) ;
#17325=CARTESIAN_POINT ( 'NONE',  ( -48.55620429048338593, -24.64965694238575011, 8.947790433994207149 ) ) ;
#17327=B_SPLINE_CURVE_WITH_KNOTS ( 'NONE', 3,
 ( #95642, #58581, #12882, #51469 ),
 .UNSPECIFIED., .F., .F.,
 ( 4, 4 ),
 ( 0.000000000000000000, 9.999999999998897304E-05 ),
 .UNSPECIFIED. ) ;
#17328=FACE_OUTER_BOUND ( 'NONE', #77138, .T. ) ;
#17329=ADVANCED_FACE ( 'NONE', ( #90836 ), #21309, .T. ) ;
#17334=EDGE_CURVE ( 'NONE', #73864, #55923, #38967, .T. ) ;
#17335=AXIS2_PLACEMENT_3D ( 'NONE', #85138, #70426, #93249 ) ;
#17336=CARTESIAN_POINT ( 'NONE',  ( -8.348131891436525009, -18.51812344263101906, 11.49999999999998934 ) ) ;
#17338=CARTESIAN_POINT ( 'NONE',  ( -34.49704148459657205, -24.15543982623907127, -0.2315651400026575435 ) ) ;
#17340=PLANE ( 'NONE',  #16836 ) ;
#17341=EDGE_CURVE ( 'NONE', #5284, #46688, #6096, .T. ) ;
#17344=CARTESIAN_POINT ( 'NONE',  ( -19.98115086844608612, 2.773124471107000666, -1.500000000000002220 ) ) ;
#17345=CARTESIAN_POINT ( 'NONE',  ( -7.741094375770895653, -19.69850519626218599, 11.49999999999999645 ) ) ;
#17346=EDGE_CURVE ( 'NONE', #78854, #61182, #35393, .T. ) ;
#17347=CARTESIAN_POINT ( 'NONE',  ( -21.57569705560537088, 4.917917830663471435, 11.49999999999998934 ) ) ;
#17348=CARTESIAN_POINT ( 'NONE',  ( -11.90445915685808131, 16.78794160864392992, -1.500000000000002220 ) ) ;
#17350=ORIENTED_EDGE ( 'NONE', *, *, #89177, .F. ) ;
#17351=CARTESIAN_POINT ( 'NONE',  ( -43.52287095715007581, -23.94994826722564696, -0.6494450866342739159 ) ) ;
#17352=ORIENTED_EDGE ( 'NONE', *, *, #64836, .T. ) ;
#17353=LINE ( 'NONE', #18357, #65769 ) ;
#17354=CARTESIAN_POINT ( 'NONE',  ( -61.62287095715007723, -24.51387760970724017, 9.387446482453425389 ) ) ;
#17355=ORIENTED_EDGE ( 'NONE', *, *, #2250, .F. ) ;
#17358=ORIENTED_EDGE ( 'NONE', *, *, #69600, .T. ) ;
#17359=CARTESIAN_POINT ( 'NONE',  ( -100.5228709571500758, -24.62226745350440282, 0.9660975649728090753 ) ) ;
#17362=CARTESIAN_POINT ( 'NONE',  ( -1.398219401198234957, 20.63772364298462847, -1.500000000000002220 ) ) ;
#17363=EDGE_CURVE ( 'NONE', #48335, #79051, #89838, .T. ) ;
#17364=CARTESIAN_POINT ( 'NONE',  ( -14.16021466491576675, 16.42052772630311352, 11.49999999999999645 ) ) ;
#17365=ORIENTED_EDGE ( 'NONE', *, *, #30265, .T. ) ;
#17369=CARTESIAN_POINT ( 'NONE',  ( 11.64234319522276095, -19.14997049866658330, -1.500000000000002220 ) ) ;
#17370=CARTESIAN_POINT ( 'NONE',  ( -47.48886131524788112, -24.51419770103156637, 9.386484678747176957 ) ) ;
#17371=CARTESIAN_POINT ( 'NONE',  ( -75.62287095715004170, -29.50248789122583659, 2.256150453626215580 ) ) ;
#17373=CARTESIAN_POINT ( 'NONE',  ( -31.62287095715006657, -23.73934037231756378, 11.05740245334329863 ) ) ;
#17374=CARTESIAN_POINT ( 'NONE',  ( -76.62287095715007013, -23.47596703998600631, 11.44779298504227860 ) ) ;
#17375=ORIENTED_EDGE ( 'NONE', *, *, #18637, .F. ) ;
#17377=DIRECTION ( 'NONE',  ( -1.000000000000000000, -3.773278334444167608E-23, -8.201307833595939069E-29 ) ) ;
#17379=ORIENTED_EDGE ( 'NONE', *, *, #49467, .T. ) ;
#17381=CARTESIAN_POINT ( 'NONE',  ( 3.302162439418223627, -20.95225242093645690, -1.500000000000002220 ) ) ;
#17382=EDGE_CURVE ( 'NONE', #40608, #60813, #39049, .T. ) ;
#17383=ORIENTED_EDGE ( 'NONE', *, *, #96285, .T. ) ;
#17384=CARTESIAN_POINT ( 'NONE',  ( -50.62889416934638120, -24.83618233451450408, 1.606449574219538601 ) ) ;
#17385=CARTESIAN_POINT ( 'NONE',  ( -1.534710021792092594, -21.76038796025502009, 11.49999999999998934 ) ) ;
#17386=CARTESIAN_POINT ( 'NONE',  ( -52.62368459130443199, -24.66019654487198665, 8.947790411086131712 ) ) ;
#17387=CARTESIAN_POINT ( 'NONE',  ( -121.5228709571500616, -29.50250243563736774, 8.947779886222134493 ) ) ;
#17388=CARTESIAN_POINT ( 'NONE',  ( -75.62287095715005592, -25.00158670708909625, 2.256160236439166855 ) ) ;
#17389=CARTESIAN_POINT ( 'NONE',  ( 0.003323472525107682655, -21.86402403546210493, -1.500000000000002220 ) ) ;
#17390=CARTESIAN_POINT ( 'NONE',  ( -30.57287095715006942, -25.14801120426701075, 3.036021546538907323 ) ) ;
#17391=ORIENTED_EDGE ( 'NONE', *, *, #81511, .F. ) ;
#17393=CARTESIAN_POINT ( 'NONE',  ( -85.58929132145466667, -24.52399227489127043, 9.353111116836526406 ) ) ;
#17397=ADVANCED_FACE ( 'NONE', ( #99436 ), #23817, .T. ) ;
#17398=ORIENTED_EDGE ( 'NONE', *, *, #49694, .T. ) ;
#17399=EDGE_CURVE ( 'NONE', #42451, #43735, #8607, .T. ) ;
#17400=ORIENTED_EDGE ( 'NONE', *, *, #97466, .T. ) ;
#17401=PLANE ( 'NONE',  #10287 ) ;
#17402=CARTESIAN_POINT ( 'NONE',  ( -113.6228709571500559, -24.34917612406837861, 0.1852690917426704775 ) ) ;
#17403=CARTESIAN_POINT ( 'NONE',  ( 20.49604761983493972, 5.601127818285958071, 11.49999999999998934 ) ) ;
#17404=PLANE ( 'NONE',  #51537 ) ;
#17405=DIRECTION ( 'NONE',  ( 3.773278334444166432E-23, -1.000000000000000000, 0.000000000000000000 ) ) ;
#17409=CARTESIAN_POINT ( 'NONE',  ( 0.06232057257353295493, 19.38168652127415825, 11.49999999999998934 ) ) ;
#17410=CARTESIAN_POINT ( 'NONE',  ( -45.48405291254921679, -24.63355581998386867, 0.9682620441943888823 ) ) ;
#17411=ORIENTED_EDGE ( 'NONE', *, *, #6348, .F. ) ;
#17412=CARTESIAN_POINT ( 'NONE',  ( -6.230579426152004885, -18.48807627814308674, 11.49999999999999645 ) ) ;
#17414=AXIS2_PLACEMENT_3D ( 'NONE', #29127, #5294, #21500 ) ;
#17416=CARTESIAN_POINT ( 'NONE',  ( -47.52287095715006160, -29.50250786944525672, 11.44777988621624054 ) ) ;
#17418=CARTESIAN_POINT ( 'NONE',  ( -103.5562042904834072, -23.47596703998600631, 11.44779298504227683 ) ) ;
#17419=CARTESIAN_POINT ( 'NONE',  ( -119.6228709571500559, -24.64965695001469115, 8.947790433994175174 ) ) ;
#17421=CARTESIAN_POINT ( 'NONE',  ( -80.77473702827948898, -25.03156056331435408, 7.542257620978359611 ) ) ;
#17422=CARTESIAN_POINT ( 'NONE',  ( -19.44079195400435012, 3.002763184081948200, 11.49999999999998934 ) ) ;
#17423=VERTEX_POINT ( 'NONE', #14197 ) ;
#17425=CARTESIAN_POINT ( 'NONE',  ( -10.32085834726444595, 20.65377284989807194, -1.500000000000002220 ) ) ;
#17428=FACE_OUTER_BOUND ( 'NONE', #93127, .T. ) ;
#17429=CARTESIAN_POINT ( 'NONE',  ( -105.5895376238167387, -23.48786465467241769, 11.44779295918253759 ) ) ;
#17430=CARTESIAN_POINT ( 'NONE',  ( -97.63001551305060843, -24.15620529776629155, 10.23563542870660115 ) ) ;
#17431=DIRECTION ( 'NONE',  ( 0.000000000000000000, 2.173523156925980399E-06, -0.9999999999976378895 ) ) ;
#17432=LINE ( 'NONE', #19799, #31183 ) ;
#17433=CARTESIAN_POINT ( 'NONE',  ( -129.6236598164479403, -24.15543982623907837, -0.2315651400026527140 ) ) ;
#17435=CARTESIAN_POINT ( 'NONE',  ( -17.57349146297605103, 9.389787994052484876, 11.49999999999998934 ) ) ;
#17436=CARTESIAN_POINT ( 'NONE',  ( -101.1706393923740848, -25.23780489406441419, 3.628358869520814434 ) ) ;
#17437=CARTESIAN_POINT ( 'NONE',  ( -15.05033210666397103, 12.90603908704162173, -1.500000000000002220 ) ) ;
#17439=DIRECTION ( 'NONE',  ( 0.000000000000000000, -2.173523156925979552E-06, 0.9999999999976378895 ) ) ;
#17440=CARTESIAN_POINT ( 'NONE',  ( -50.93420549988994139, -25.14762240475955579, 7.017504830804345062 ) ) ;
#17441=CARTESIAN_POINT ( 'NONE',  ( -42.52287095715005449, -23.47593901973090169, -1.443836447538997092 ) ) ;
#17442=CARTESIAN_POINT ( 'NONE',  ( 15.70846742882596025, 13.54617332914617478, 11.49999999999999645 ) ) ;
#17445=CARTESIAN_POINT ( 'NONE',  ( 22.80427751693360960, 0.003464389817739472934, 11.49999999999999645 ) ) ;
#17446=ORIENTED_EDGE ( 'NONE', *, *, #20572, .T. ) ;
#17447=EDGE_CURVE ( 'NONE', #21027, #32109, #20802, .T. ) ;
#17448=B_SPLINE_SURFACE_WITH_KNOTS ( 'NONE', 3, 3, ( 
 ( #22840, #61939, #85767, #62438 ),
 ( #54331, #85257, #23856, #46714 ),
 ( #54832, #10648, #25869, #18746 ),
 ( #48728, #56342, #41106, #26870 ),
 ( #49230, #50214, #81659, #4040 ),
 ( #33984, #26371, #95380, #41610 ),
 ( #72062, #10144, #96379, #50709 ) ),
 .UNSPECIFIED., .F., .F., .F.,
 ( 4, 3, 4 ),
 ( 4, 4 ),
 ( 0.0004766839783834151811, 0.1029713700210900668, 0.2054660560637967259 ),
 ( 0.9197279603282626503, 0.9211650456752530358 ),
 .UNSPECIFIED. ) ;
#17449=CARTESIAN_POINT ( 'NONE',  ( -69.58397737201534028, -24.51314013834315375, 0.6176544820404143987 ) ) ;
#17450=PLANE ( 'NONE',  #66320 ) ;
#17452=CARTESIAN_POINT ( 'NONE',  ( -2.107266074560359748, -20.09985696230311447, 11.49999999999998934 ) ) ;
#17453=CARTESIAN_POINT ( 'NONE',  ( -106.5228709571500332, -23.73934037231757443, 11.05740245334327732 ) ) ;
#17454=CARTESIAN_POINT ( 'NONE',  ( -114.6228709571500559, -24.66019654487199730, 8.947790411086122830 ) ) ;
#17456=EDGE_CURVE ( 'NONE', #13848, #91650, #80122, .T. ) ;
#17457=VECTOR ( 'NONE', #86683, 1000.000000000000114 ) ;
#17458=EDGE_CURVE ( 'NONE', #25716, #30457, #54790, .T. ) ;
#17459=ORIENTED_EDGE ( 'NONE', *, *, #13451, .F. ) ;
#17460=CARTESIAN_POINT ( 'NONE',  ( -70.62287095715007013, -23.47596703998600631, 11.44779298504227505 ) ) ;
#17461=CARTESIAN_POINT ( 'NONE',  ( -51.62287095715008434, -24.34917612406837861, 0.1852690917426609851 ) ) ;
#17462=CARTESIAN_POINT ( 'NONE',  ( 13.87436705529610492, 14.39054836566213780, -1.500000000000002220 ) ) ;
#17464=CARTESIAN_POINT ( 'NONE',  ( -18.08314111433443827, -10.61732331186343004, 11.49999999999999645 ) ) ;
#17465=EDGE_CURVE ( 'NONE', #26092, #95938, #43818, .T. ) ;
#17468=CARTESIAN_POINT ( 'NONE',  ( -8.753671783739276790, -20.25744411100385634, -1.500000000000002220 ) ) ;
#17469=VECTOR ( 'NONE', #83370, 1000.000000000000114 ) ;
#17471=VERTEX_POINT ( 'NONE', #46168 ) ;
#17473=CARTESIAN_POINT ( 'NONE',  ( -118.5228709571501184, -24.51387760970726504, 9.387446482453404073 ) ) ;
#17474=CARTESIAN_POINT ( 'NONE',  ( -81.62287095715005592, -29.50247984919015209, -1.443849546365053582 ) ) ;
#17479=EDGE_LOOP ( 'NONE', ( #80406, #27833, #8015, #80902 ) ) ;
#17480=CARTESIAN_POINT ( 'NONE',  ( -78.92287095715010992, -23.47593901973090524, -1.443836447538997980 ) ) ;
#17481=FACE_OUTER_BOUND ( 'NONE', #84862, .T. ) ;
#17482=CARTESIAN_POINT ( 'NONE',  ( -122.6228709571500417, -23.48786465467242124, 11.44779295918253759 ) ) ;
#17483=CARTESIAN_POINT ( 'NONE',  ( -20.49763986188970932, -1.003951800832726615, -1.500000000000002220 ) ) ;
#17485=EDGE_LOOP ( 'NONE', ( #98872, #2665, #49966, #57724 ) ) ;
#17486=CARTESIAN_POINT ( 'NONE',  ( -71.62287095715005592, -23.48786465467241413, 11.44779295918254469 ) ) ;
#17489=CARTESIAN_POINT ( 'NONE',  ( -16.35649155429130985, -15.18990082740072367, 11.49999999999998934 ) ) ;
#17490=CARTESIAN_POINT ( 'NONE',  ( -0.008165992925886831136, -22.94428480439657392, 3.856996771331003160 ) ) ;
#17491=LINE ( 'NONE', #46950, #72328 ) ;
#17492=EDGE_CURVE ( 'NONE', #39531, #62936, #98257, .T. ) ;
#17497=CARTESIAN_POINT ( 'NONE',  ( -0.6367455441941621830, -20.85161220577290919, 11.49999999999998934 ) ) ;
#17498=ORIENTED_EDGE ( 'NONE', *, *, #54021, .T. ) ;
#17502=ORIENTED_EDGE ( 'NONE', *, *, #65379, .T. ) ;
#17503=B_SPLINE_CURVE_WITH_KNOTS ( 'NONE', 3,
 ( #67941, #52706, #22727, #23234 ),
 .UNSPECIFIED., .F., .F.,
 ( 4, 4 ),
 ( 0.000000000000000000, 0.0001000000000000028644 ),
 .UNSPECIFIED. ) ;
#17505=CARTESIAN_POINT ( 'NONE',  ( 12.48895993392301307, -16.95307763291877379, -1.500000000000002220 ) ) ;
#17506=ORIENTED_EDGE ( 'NONE', *, *, #21802, .F. ) ;
#17507=CARTESIAN_POINT ( 'NONE',  ( -37.55620429048341435, -24.64965694238574656, 8.947790433994205372 ) ) ;
#17509=FACE_OUTER_BOUND ( 'NONE', #2033, .T. ) ;
#17510=CARTESIAN_POINT ( 'NONE',  ( -101.9401486745561272, -25.25419277357474712, 6.289339016573623375 ) ) ;
#17511=CARTESIAN_POINT ( 'NONE',  ( -59.49823463814401237, -24.34968618360933235, 0.1864209137778795600 ) ) ;
#17512=CARTESIAN_POINT ( 'NONE',  ( -109.0819061167040047, -25.31465039088007174, 4.788656490444584080 ) ) ;
#17514=CARTESIAN_POINT ( 'NONE',  ( -21.61287440533560300, 5.199345243644041936, 11.49999999999999645 ) ) ;
#17515=VERTEX_POINT ( 'NONE', #47174 ) ;
#17516=CARTESIAN_POINT ( 'NONE',  ( -120.5228709571500616, -29.50250786944525672, 11.44777988621622811 ) ) ;
#17517=CARTESIAN_POINT ( 'NONE',  ( -37.52287095715006870, -23.48786465467240347, 11.44779295918255180 ) ) ;
#17519=B_SPLINE_CURVE_WITH_KNOTS ( 'NONE', 3,
 ( #38739, #70200, #31630, #61609 ),
 .UNSPECIFIED., .F., .F.,
 ( 4, 4 ),
 ( 0.000000000000000000, 9.999999999998206125E-05 ),
 .UNSPECIFIED. ) ;
#17520=CARTESIAN_POINT ( 'NONE',  ( 17.73637878876437668, -14.10177982315242318, 11.49999999999998934 ) ) ;
#17521=ADVANCED_FACE ( 'NONE', ( #994 ), #84672, .T. ) ;
#17522=DIRECTION ( 'NONE',  ( -3.773278334453079030E-23, 0.9999999999976377785, 2.173523156925979128E-06 ) ) ;
#17527=CARTESIAN_POINT ( 'NONE',  ( -17.16780662754360520, -10.58209718439171176, 11.49999999999998934 ) ) ;
#17528=CARTESIAN_POINT ( 'NONE',  ( -105.5228709571501184, -24.15431212366389957, -0.2830839119429224837 ) ) ;
#17529=ORIENTED_EDGE ( 'NONE', *, *, #74867, .T. ) ;
#17531=CARTESIAN_POINT ( 'NONE',  ( -14.11974515630795501, -17.41659395067913962, -1.500000000000002220 ) ) ;
#17532=ORIENTED_EDGE ( 'NONE', *, *, #61716, .T. ) ;
#17534=CARTESIAN_POINT ( 'NONE',  ( -112.6299582353932607, -23.73791477778912551, 11.05961554403169878 ) ) ;
#17536=CARTESIAN_POINT ( 'NONE',  ( -61.52287095715006160, -23.47596703998600631, 11.44779298504228926 ) ) ;
#17537=CARTESIAN_POINT ( 'NONE',  ( -98.62287095715005592, -29.50247984919015209, -1.443849546365050029 ) ) ;
#17538=VECTOR ( 'NONE', #41911, 1000.000000000000114 ) ;
#17540=CARTESIAN_POINT ( 'NONE',  ( -0.9579564967699066846, 19.55851204243107233, 11.49999999999998934 ) ) ;
#17541=CARTESIAN_POINT ( 'NONE',  ( -49.97243670601686460, -25.31053666847986960, 4.650320011491689165 ) ) ;
#17543=CARTESIAN_POINT ( 'NONE',  ( -0.7226137440361984909, -21.50112622129444162, 11.49999999999998934 ) ) ;
#17544=B_SPLINE_CURVE_WITH_KNOTS ( 'NONE', 3,
 ( #17460, #78346, #47418, #24563, #1743, #26074, #72266, #2754 ),
 .UNSPECIFIED., .F., .F.,
 ( 4, 2, 2, 4 ),
 ( 0.000000000000000000, 0.002001079623178223660, 0.003001619434767337224, 0.004002159246356450789 ),
 .UNSPECIFIED. ) ;
#17545=PLANE ( 'NONE',  #41479 ) ;
#17546=CARTESIAN_POINT ( 'NONE',  ( -121.5228709571500474, -24.34917612406837151, 0.1852690917426603190 ) ) ;
#17547=CARTESIAN_POINT ( 'NONE',  ( -123.5228709571501184, -24.66019654487200441, 8.947790411086105067 ) ) ;
#17549=CARTESIAN_POINT ( 'NONE',  ( 21.13568926591755925, -8.834425160694816981, -1.500000000000002220 ) ) ;
#17552=B_SPLINE_CURVE_WITH_KNOTS ( 'NONE', 3,
 ( #53468, #30105, #91503, #84893 ),
 .UNSPECIFIED., .F., .F.,
 ( 4, 4 ),
 ( 0.000000000000000000, 9.999999999998206125E-05 ),
 .UNSPECIFIED. ) ;
#17554=PLANE ( 'NONE',  #47423 ) ;
#17555=CARTESIAN_POINT ( 'NONE',  ( -19.91332876899582160, 2.521106391696132931, 11.49999999999999645 ) ) ;
#17559=CARTESIAN_POINT ( 'NONE',  ( -88.62287095715004170, -23.47593901973091235, -1.443836447539002865 ) ) ;
#17560=LINE ( 'NONE', #1346, #34326 ) ;
#17561=DIRECTION ( 'NONE',  ( -3.773278334453079030E-23, 0.9999999999976377785, 2.173523156925979128E-06 ) ) ;
#17562=CARTESIAN_POINT ( 'NONE',  ( 19.75055111929153639, -1.948201398878238066, -1.500000000000002220 ) ) ;
#17563=CARTESIAN_POINT ( 'NONE',  ( 11.36066313177254905, -18.55813952095733654, -1.500000000000002220 ) ) ;
#17565=CARTESIAN_POINT ( 'NONE',  ( 13.00645856128228495, 14.71372164842801844, -1.500000000000002220 ) ) ;
#17567=CARTESIAN_POINT ( 'NONE',  ( -121.6228709571500559, -23.47596703998600631, 11.44779298504227683 ) ) ;
#17570=CARTESIAN_POINT ( 'NONE',  ( 17.96566822227200433, 9.963707542159163211, 11.49999999999999645 ) ) ;
#17572=CARTESIAN_POINT ( 'NONE',  ( -47.62287095715004170, -23.73907113216990794, -1.053371485793233697 ) ) ;
#17573=CARTESIAN_POINT ( 'NONE',  ( 15.88279217892459094, 16.07415641707351384, 11.49999999999999645 ) ) ;
#17574=ORIENTED_EDGE ( 'NONE', *, *, #16602, .T. ) ;
#17575=CARTESIAN_POINT ( 'NONE',  ( -45.52287095715006160, -29.50249982740957577, 7.747779886224967605 ) ) ;
#17577=CARTESIAN_POINT ( 'NONE',  ( -97.51608943600319890, -23.96119346886881374, -0.6495511937832056937 ) ) ;
#17579=CARTESIAN_POINT ( 'NONE',  ( -27.54213053348642504, -24.77237661284991432, 2.282611211521436534 ) ) ;
#17580=EDGE_CURVE ( 'NONE', #93616, #30931, #93406, .T. ) ;
#17582=EDGE_CURVE ( 'NONE', #16907, #44949, #24321, .T. ) ;
#17583=DIRECTION ( 'NONE',  ( -3.773278334453079618E-23, 0.9999999999976377785, 2.173523156925979975E-06 ) ) ;
#17584=EDGE_CURVE ( 'NONE', #8126, #34234, #63918, .T. ) ;
#17585=EDGE_LOOP ( 'NONE', ( #75689, #43862, #36169, #85197 ) ) ;
#17586=CARTESIAN_POINT ( 'NONE',  ( -79.41916052885848387, -25.26750005083801653, 5.559759467608911265 ) ) ;
#17587=CARTESIAN_POINT ( 'NONE',  ( 16.54545882101025711, 15.75737887292823558, 11.49999999999998934 ) ) ;
#17589=B_SPLINE_CURVE_WITH_KNOTS ( 'NONE', 3,
 ( #76620, #14729, #83247, #90863 ),
 .UNSPECIFIED., .F., .F.,
 ( 4, 4 ),
 ( 6.938893903907228378E-18, 9.999999999999591193E-05 ),
 .UNSPECIFIED. ) ;
#17590=CARTESIAN_POINT ( 'NONE',  ( -115.5228709571500616, -24.99156044556202616, 7.747789690856173195 ) ) ;
#17591=CARTESIAN_POINT ( 'NONE',  ( -63.63170045961884114, -24.35071581493543036, 9.817618358456027039 ) ) ;
#17592=CARTESIAN_POINT ( 'NONE',  ( 21.70358988458699301, 5.938112137899119070, 11.49999999999999645 ) ) ;
#17593=ORIENTED_EDGE ( 'NONE', *, *, #29623, .T. ) ;
#17594=LINE ( 'NONE', #2380, #35160 ) ;
#17595=CARTESIAN_POINT ( 'NONE',  ( -20.77788740438921522, -7.151594987469691134, -1.500000000000002220 ) ) ;
#17597=B_SPLINE_CURVE_WITH_KNOTS ( 'NONE', 3,
 ( #91981, #46311, #31074, #38186 ),
 .UNSPECIFIED., .F., .F.,
 ( 4, 4 ),
 ( 0.000000000000000000, 0.0001000000000000167422 ),
 .UNSPECIFIED. ) ;
#17598=CARTESIAN_POINT ( 'NONE',  ( -34.62916631692677782, -24.51419770103156637, 9.386484678747176957 ) ) ;
#17602=CARTESIAN_POINT ( 'NONE',  ( -48.62833534578886940, -24.51419770103156637, 9.386484678747178734 ) ) ;
#17603=DIRECTION ( 'NONE',  ( 0.000000000000000000, -0.9999999999976377785, -2.173523156925979128E-06 ) ) ;
#17605=CARTESIAN_POINT ( 'NONE',  ( -15.16157141410761966, -13.82251119679066953, -1.500000000000002220 ) ) ;
#17607=ORIENTED_EDGE ( 'NONE', *, *, #27550, .T. ) ;
#17608=ORIENTED_EDGE ( 'NONE', *, *, #97413, .T. ) ;
#17610=CARTESIAN_POINT ( 'NONE',  ( -81.33773576950629547, -25.20044588977664546, 6.673200621925437837 ) ) ;
#17611=CARTESIAN_POINT ( 'NONE',  ( 21.06059016766346659, 9.494407541345388779, -1.500000000000002220 ) ) ;
#17613=CARTESIAN_POINT ( 'NONE',  ( -13.46841296510753061, 15.22696965993213070, -1.500000000000002220 ) ) ;
#17614=ORIENTED_EDGE ( 'NONE', *, *, #60836, .F. ) ;
#17618=CARTESIAN_POINT ( 'NONE',  ( -114.6228709571500701, -24.51387760970725083, 9.387446482453411178 ) ) ;
#17620=CARTESIAN_POINT ( 'NONE',  ( -21.25412285906045895, 3.082840150875858054, 11.49999999999999645 ) ) ;
#17621=ORIENTED_EDGE ( 'NONE', *, *, #1889, .T. ) ;
#17622=CARTESIAN_POINT ( 'NONE',  ( -75.62719845405518981, -24.83618233451450763, 1.606449574219540599 ) ) ;
#17623=CARTESIAN_POINT ( 'NONE',  ( -48.62287095715004881, -24.64898659630528144, 1.056161002820821038 ) ) ;
#17624=ORIENTED_EDGE ( 'NONE', *, *, #42921, .F. ) ;
#17625=CARTESIAN_POINT ( 'NONE',  ( 3.485566553294195291, 20.44204155273375889, -1.500000000000002220 ) ) ;
#17628=ORIENTED_EDGE ( 'NONE', *, *, #100335, .T. ) ;
#17629=CARTESIAN_POINT ( 'NONE',  ( -77.52287095715010423, -23.47593901973090524, -1.443836447538997092 ) ) ;
#17630=CARTESIAN_POINT ( 'NONE',  ( -97.52287095715006160, -23.48786465467241769, 11.44779295918254114 ) ) ;
#17631=ORIENTED_EDGE ( 'NONE', *, *, #88871, .T. ) ;
#17632=VERTEX_POINT ( 'NONE', #95336 ) ;
#17635=CARTESIAN_POINT ( 'NONE',  ( -42.48684989586963923, -24.51419770103158413, 9.386484678747191168 ) ) ;
#17636=CARTESIAN_POINT ( 'NONE',  ( -28.67183314889459922, -24.76456359476621216, 1.897690051802386924 ) ) ;
#17637=CARTESIAN_POINT ( 'NONE',  ( -16.14483305390557888, 14.99321182834783528, 11.49999999999999645 ) ) ;
#17639=CARTESIAN_POINT ( 'NONE',  ( -48.98794818101416837, -25.19490310348271578, 6.713761956252816354 ) ) ;
#17640=CARTESIAN_POINT ( 'NONE',  ( 11.79716412695777272, 19.27136520130675024, -1.500000000000002220 ) ) ;
#17641=CARTESIAN_POINT ( 'NONE',  ( 20.40321384664088811, -4.974606123342796060, -1.500000000000002220 ) ) ;
#17642=CARTESIAN_POINT ( 'NONE',  ( -70.62287095715009855, -24.62226745350439927, 0.9660975649728139603 ) ) ;
#17643=ORIENTED_EDGE ( 'NONE', *, *, #23500, .F. ) ;
#17644=VERTEX_POINT ( 'NONE', #64918 ) ;
#17647=B_SPLINE_CURVE_WITH_KNOTS ( 'NONE', 3,
 ( #65076, #87376, #48834, #57951 ),
 .UNSPECIFIED., .F., .F.,
 ( 4, 4 ),
 ( 2.775557561562891043E-17, 9.999999999996124456E-05 ),
 .UNSPECIFIED. ) ;
#17650=VERTEX_POINT ( 'NONE', #94832 ) ;
#17651=CARTESIAN_POINT ( 'NONE',  ( 17.87031378931267867, -11.31994873005049129, -1.500000000000002220 ) ) ;
#17653=CARTESIAN_POINT ( 'NONE',  ( -50.91781549829847364, -25.26041104471375576, 7.505037088851381100 ) ) ;
#17654=CARTESIAN_POINT ( 'NONE',  ( -32.58953762381673869, -23.47596703998600276, 11.44779298504227505 ) ) ;
#17656=CARTESIAN_POINT ( 'NONE',  ( 4.129723114849880083, -21.82631191821171512, -1.500000000000002220 ) ) ;
#17657=CARTESIAN_POINT ( 'NONE',  ( -74.62287095715002749, -24.33927499327855060, 9.819080762295817166 ) ) ;
#17659=CARTESIAN_POINT ( 'NONE',  ( -112.5228709571500616, -24.65952944569304961, 1.056160979905704123 ) ) ;
#17660=CARTESIAN_POINT ( 'NONE',  ( -64.62287095715007013, -23.47596703998600631, 11.44779298504227683 ) ) ;
#17661=CARTESIAN_POINT ( 'NONE',  ( 15.46825748771582631, 11.69065726450791409, 11.49999999999999645 ) ) ;
#17662=CARTESIAN_POINT ( 'NONE',  ( -36.52731531746556470, -24.66019654487199730, 8.947790411086113949 ) ) ;
#17663=B_SPLINE_CURVE_WITH_KNOTS ( 'NONE', 3,
 ( #64259, #56134, #23651, #70848, #25665, #93161, #47513, #15543, #827, #71351, #33272, #9435, #78438, #8441 ),
 .UNSPECIFIED., .F., .F.,
 ( 4, 2, 2, 2, 2, 2, 4 ),
 ( 0.000000000000000000, 0.0001813126694408965036, 0.0003626253388817930073, 0.0007252506777635843883, 0.001087876016645375823, 0.001269188686086291382, 0.001450501355527207374 ),
 .UNSPECIFIED. ) ;
#17664=CARTESIAN_POINT ( 'NONE',  ( -39.58953762381673158, -24.64965694238574656, 8.947790433994203596 ) ) ;
#17665=CARTESIAN_POINT ( 'NONE',  ( -2.678125609936932605, 19.29598960679622976, -1.500000000000002220 ) ) ;
#17666=CARTESIAN_POINT ( 'NONE',  ( -21.42254595866439004, -0.3319015934494286557, -1.500000000000002220 ) ) ;
#17668=CARTESIAN_POINT ( 'NONE',  ( -60.58606081320825609, -24.63419186845290199, 9.035850630957110496 ) ) ;
#17669=CARTESIAN_POINT ( 'NONE',  ( -51.56024018657757324, -23.73766607897669445, -1.055555164236457788 ) ) ;
#17670=CARTESIAN_POINT ( 'NONE',  ( -77.58172370980747701, -24.65952944569304606, 1.056160979905701458 ) ) ;
#17671=CARTESIAN_POINT ( 'NONE',  ( -22.77908990650604792, -0.06651829912971220227, -1.500000000000002220 ) ) ;
#17673=CARTESIAN_POINT ( 'NONE',  ( -102.5094055064049172, -24.65952944569305316, 1.056160979905704123 ) ) ;
#17675=CARTESIAN_POINT ( 'NONE',  ( -5.703961651189128901, -19.02375728206049743, 11.49999999999999645 ) ) ;
#17676=CARTESIAN_POINT ( 'NONE',  ( -84.52287095715006160, -24.65952944569304606, 1.056160979905698794 ) ) ;
#17677=AXIS2_PLACEMENT_3D ( 'NONE', #86099, #16577, #47553 ) ;
#17679=CARTESIAN_POINT ( 'NONE',  ( -89.06226385320384509, -25.27880950044345809, 5.947789066509452383 ) ) ;
#17681=ORIENTED_EDGE ( 'NONE', *, *, #16702, .T. ) ;
#17682=CARTESIAN_POINT ( 'NONE',  ( -84.52287095715006160, -29.50250786944525672, 11.44777988621623521 ) ) ;
#17684=CARTESIAN_POINT ( 'NONE',  ( -51.19185979282234200, -25.10935809339517633, 3.072504015734757843 ) ) ;
#17685=CARTESIAN_POINT ( 'NONE',  ( -21.58526226860004371, 1.989002153404973328, 11.49999999999998934 ) ) ;
#17686=CARTESIAN_POINT ( 'NONE',  ( -67.52287095715006160, -24.65952944569304961, 1.056160979905697239 ) ) ;
#17688=CARTESIAN_POINT ( 'NONE',  ( -11.39837868854680814, -15.77482985264681403, -1.500000000000002220 ) ) ;
#17693=CARTESIAN_POINT ( 'NONE',  ( -12.60687543931603471, -16.05746371069360379, 11.49999999999999645 ) ) ;
#17694=DIRECTION ( 'NONE',  ( 0.000000000000000000, -2.173523156925979552E-06, 0.9999999999976378895 ) ) ;
#17696=B_SPLINE_CURVE_WITH_KNOTS ( 'NONE', 3,
 ( #32512, #72587, #78661, #5555, #11665, #4069 ),
 .UNSPECIFIED., .F., .F.,
 ( 4, 2, 4 ),
 ( 0.000000000000000000, 0.001380764517854764532, 0.002761529035709529064 ),
 .UNSPECIFIED. ) ;
#17698=CARTESIAN_POINT ( 'NONE',  ( -41.24483612983362946, -25.23676607602647337, 3.617455962827678562 ) ) ;
#17700=CARTESIAN_POINT ( 'NONE',  ( -39.10567952407142656, -25.27985361285174903, 4.652296651879083811 ) ) ;
#17701=EDGE_CURVE ( 'NONE', #47794, #43355, #45096, .T. ) ;
#17702=AXIS2_PLACEMENT_3D ( 'NONE', #83097, #21201, #13087 ) ;
#17705=PLANE ( 'NONE',  #14344 ) ;
#17707=ORIENTED_EDGE ( 'NONE', *, *, #15686, .F. ) ;
#17709=EDGE_CURVE ( 'NONE', #84649, #27354, #3944, .T. ) ;
#17710=CARTESIAN_POINT ( 'NONE',  ( -21.48638390452810043, -8.140844714011898020, 11.49999999999999645 ) ) ;
#17711=CARTESIAN_POINT ( 'NONE',  ( 22.67573665902413182, 1.879276792517311501, 11.49999999999998934 ) ) ;
#17713=CARTESIAN_POINT ( 'NONE',  ( -110.6256069007815626, -24.73531770709095312, 8.716586749053508498 ) ) ;
#17715=CARTESIAN_POINT ( 'NONE',  ( -75.62287095715009855, -24.63345952396255356, 9.038047939301504741 ) ) ;
#17718=LINE ( 'NONE', #63920, #85409 ) ;
#17719=CARTESIAN_POINT ( 'NONE',  ( -18.33957545910867282, 11.93505917737106259, -1.500000000000002220 ) ) ;
#17720=CARTESIAN_POINT ( 'NONE',  ( -74.52287095715007581, -23.47593901973090169, -1.443836447538996870 ) ) ;
#17724=FACE_OUTER_BOUND ( 'NONE', #65092, .T. ) ;
#17726=CARTESIAN_POINT ( 'NONE',  ( 19.51578053514377586, 5.923290232019536639, -1.500000000000002220 ) ) ;
#17727=ORIENTED_EDGE ( 'NONE', *, *, #87572, .T. ) ;
#17730=CARTESIAN_POINT ( 'NONE',  ( 17.37538969058663696, -15.08583811485692117, 11.49999999999998934 ) ) ;
#17732=ORIENTED_EDGE ( 'NONE', *, *, #73825, .T. ) ;
#17733=CARTESIAN_POINT ( 'NONE',  ( -101.5228709571500758, -24.65952944569304606, 1.056160979905702346 ) ) ;
#17735=CARTESIAN_POINT ( 'NONE',  ( -95.55372101787112626, -24.15503026093913874, -0.2815557561904519224 ) ) ;
#17737=CARTESIAN_POINT ( 'NONE',  ( 3.515848477382193416, 21.04717058667041130, 11.49999999999999645 ) ) ;
#17739=EDGE_LOOP ( 'NONE', ( #65063, #64202, #3667, #73022 ) ) ;
#17740=CARTESIAN_POINT ( 'NONE',  ( -11.95080204275630464, 18.75100984808165094, -1.500000000000002220 ) ) ;
#17741=CARTESIAN_POINT ( 'NONE',  ( 19.39950376024442846, -7.079068461131618584, 11.49999999999998934 ) ) ;
#17744=CARTESIAN_POINT ( 'NONE',  ( -95.54323508187783887, -24.92592662359561473, 8.075495903017998245 ) ) ;
#17749=CARTESIAN_POINT ( 'NONE',  ( -49.55620429048340014, -23.48783264082477729, -1.443836473390071484 ) ) ;
#17751=CARTESIAN_POINT ( 'NONE',  ( -10.06633388967972209, 18.29571535785830960, -1.500000000000002220 ) ) ;
#17752=CARTESIAN_POINT ( 'NONE',  ( -9.708950231915746798, -19.59419465507263070, 11.49999999999999645 ) ) ;
#17753=EDGE_CURVE ( 'NONE', #58220, #37557, #95832, .T. ) ;
#17754=CARTESIAN_POINT ( 'NONE',  ( -107.6228709571501412, -24.35013146730204525, 9.818937971375106599 ) ) ;
#17756=CARTESIAN_POINT ( 'NONE',  ( -9.984083066403742990, 20.14924292131567185, 11.49999999999998934 ) ) ;
#17757=VECTOR ( 'NONE', #58565, 1000.000000000000114 ) ;
#17758=CARTESIAN_POINT ( 'NONE',  ( 13.94627346685978075, -15.57361473980792255, -1.500000000000002220 ) ) ;
#17759=CARTESIAN_POINT ( 'NONE',  ( -89.40841769935771310, -25.35030500980171553, 4.902495265462817997 ) ) ;
#17761=CARTESIAN_POINT ( 'NONE',  ( -72.52287095715009002, -24.35013146730203815, 9.818937971375110152 ) ) ;
#17763=VERTEX_POINT ( 'NONE', #19692 ) ;
#17767=EDGE_LOOP ( 'NONE', ( #99402, #4135, #8734, #20321 ) ) ;
#17768=CARTESIAN_POINT ( 'NONE',  ( -99.29890324015507019, -25.12215488674418751, 6.243173985830122064 ) ) ;
#17769=ORIENTED_EDGE ( 'NONE', *, *, #40629, .T. ) ;
#17770=VECTOR ( 'NONE', #15497, 1000.000000000000114 ) ;
#17771=CARTESIAN_POINT ( 'NONE',  ( 6.029407872858970840, -20.54391778677962677, -1.500000000000002220 ) ) ;
#17772=CARTESIAN_POINT ( 'NONE',  ( -11.68221627493902126, 19.09626523228051553, 11.49999999999999645 ) ) ;
#17773=EDGE_CURVE ( 'NONE', #25724, #12032, #82601, .T. ) ;
#17775=CARTESIAN_POINT ( 'NONE',  ( -26.33488822642538452, -24.88201932036028552, 6.524121876823151034 ) ) ;
#17776=CARTESIAN_POINT ( 'NONE',  ( 20.75205275252385206, -3.532026382766447536, -1.500000000000002220 ) ) ;
#17777=CARTESIAN_POINT ( 'NONE',  ( -30.54990185496676247, -24.48551988174978078, 9.440108529385042857 ) ) ;
#17778=CARTESIAN_POINT ( 'NONE',  ( -18.79874323561663729, 6.599581278811135654, -1.500000000000002220 ) ) ;
#17780=CARTESIAN_POINT ( 'NONE',  ( -101.5910278892822447, -24.15543982623907482, -0.2315651400026588480 ) ) ;
#17781=CARTESIAN_POINT ( 'NONE',  ( -7.807709442696729063, 20.60712426125841645, -1.500000000000002220 ) ) ;
#17785=CARTESIAN_POINT ( 'NONE',  ( -96.62287095715005592, -23.48786465467241413, 11.44779295918254114 ) ) ;
#17786=CARTESIAN_POINT ( 'NONE',  ( -4.186882374726557110, 20.40937146592452223, 11.49999999999999645 ) ) ;
#17787=CARTESIAN_POINT ( 'NONE',  ( -25.50529870902546037, -24.92367794922509816, 4.936952632524853612 ) ) ;
#17789=CARTESIAN_POINT ( 'NONE',  ( -129.6228709571500417, -29.50247984919015209, -1.443849546365044922 ) ) ;
#17790=CARTESIAN_POINT ( 'NONE',  ( -6.196366259867160942, 20.41550611124569059, -1.500000000000002220 ) ) ;
#17792=CARTESIAN_POINT ( 'NONE',  ( -66.62287095715005592, -23.47596703998600276, 11.44779298504227683 ) ) ;
#17793=DIRECTION ( 'NONE',  ( -0.000000000000000000, 2.173523156925979552E-06, -0.9999999999976378895 ) ) ;
#17794=PLANE ( 'NONE',  #588 ) ;
#17796=CARTESIAN_POINT ( 'NONE',  ( -8.633696204196466439, -20.85254729778420923, -1.500000000000002220 ) ) ;
#17797=B_SPLINE_CURVE_WITH_KNOTS ( 'NONE', 3,
 ( #99797, #55670, #1378, #7464 ),
 .UNSPECIFIED., .F., .F.,
 ( 4, 4 ),
 ( 2.775557561562891043E-17, 9.999999999998898659E-05 ),
 .UNSPECIFIED. ) ;
#17798=CARTESIAN_POINT ( 'NONE',  ( -81.62287095715005592, -24.65952944569304606, 1.056160979905699460 ) ) ;
#17800=FACE_OUTER_BOUND ( 'NONE', #74578, .T. ) ;
#17801=CARTESIAN_POINT ( 'NONE',  ( -31.57095388386905199, -23.48786465467240347, 11.44779295918255535 ) ) ;
#17802=CARTESIAN_POINT ( 'NONE',  ( 2.289404864003111051, -19.52285375609543294, 11.49999999999999645 ) ) ;
#17805=B_SPLINE_CURVE_WITH_KNOTS ( 'NONE', 3,
 ( #19325, #44677, #29432, #45673 ),
 .UNSPECIFIED., .F., .F.,
 ( 4, 4 ),
 ( 0.8694025111800981476, 0.8704032582208635072 ),
 .UNSPECIFIED. ) ;
#17807=CARTESIAN_POINT ( 'NONE',  ( -94.52287095715011844, -23.48783264082477373, -1.443836473390087027 ) ) ;
#17808=CARTESIAN_POINT ( 'NONE',  ( -55.62287095715003460, -24.82558206586145033, 1.605769216559449930 ) ) ;
#17809=DIRECTION ( 'NONE',  ( -3.773278334453079618E-23, 0.9999999999976377785, 2.173523156925979975E-06 ) ) ;
#17811=CARTESIAN_POINT ( 'NONE',  ( -32.50560602629348494, -24.87219037988797865, 1.747789950295646877 ) ) ;
#17813=CARTESIAN_POINT ( 'NONE',  ( 14.33573519231038063, 13.56928687979844561, 11.49999999999998934 ) ) ;
#17814=EDGE_LOOP ( 'NONE', ( #74627, #78113, #98297, #87365 ) ) ;
#17815=CARTESIAN_POINT ( 'NONE',  ( 20.15506735835773000, -1.303320585059813741, 11.49999999999999645 ) ) ;
#17819=CARTESIAN_POINT ( 'NONE',  ( -67.52287095715006160, -23.48786465467241769, 11.44779295918254647 ) ) ;
#17820=CARTESIAN_POINT ( 'NONE',  ( -69.34990230688175927, -25.25756224058122967, 6.083752085800076870 ) ) ;
#17821=CARTESIAN_POINT ( 'NONE',  ( -88.88918693012689687, -25.27880950044345454, 5.947789066509454159 ) ) ;
#17822=CARTESIAN_POINT ( 'NONE',  ( -38.52287095715006870, -24.64898659630367206, 1.056161002820819261 ) ) ;
#17824=CARTESIAN_POINT ( 'NONE',  ( -103.6228709571501128, -23.95044443724992789, 10.65354141964649592 ) ) ;
#17826=CARTESIAN_POINT ( 'NONE',  ( 7.431233518514567926, -18.57414813805618081, -1.500000000000002220 ) ) ;
#17828=CARTESIAN_POINT ( 'NONE',  ( -99.62559895716422886, -25.27532914723576241, 3.076829306349715853 ) ) ;
#17832=CARTESIAN_POINT ( 'NONE',  ( -79.49884268526720632, -24.66019654487199375, 8.947790411086119278 ) ) ;
#17833=ADVANCED_FACE ( 'NONE', ( #57786 ), #28315, .T. ) ;
#17837=EDGE_CURVE ( 'NONE', #93974, #1915, #70226, .T. ) ;
#17838=CARTESIAN_POINT ( 'NONE',  ( -119.4336609825042927, -25.40057329150818077, 4.607792141311822576 ) ) ;
#17839=CARTESIAN_POINT ( 'NONE',  ( -103.5228709571500900, -23.96127896941633395, -0.6493128931038035789 ) ) ;
#17842=CARTESIAN_POINT ( 'NONE',  ( -75.62287095715004170, -29.50249982740957577, 7.747779886224967605 ) ) ;
#17843=VERTEX_POINT ( 'NONE', #21191 ) ;
#17844=CARTESIAN_POINT ( 'NONE',  ( 13.49383759531269433, -15.17088004136028090, -1.500000000000002220 ) ) ;
#17848=CARTESIAN_POINT ( 'NONE',  ( -127.5210440253001849, -24.51419770103158768, 9.386484678747160970 ) ) ;
#17849=CARTESIAN_POINT ( 'NONE',  ( -59.54824621938957563, -24.15620529776628089, 10.23563542870661180 ) ) ;
#17851=B_SPLINE_CURVE_WITH_KNOTS ( 'NONE', 3,
 ( #83328, #13808, #81344, #11825 ),
 .UNSPECIFIED., .F., .F.,
 ( 4, 4 ),
 ( 2.775557561562891351E-17, 0.0001000000000000167286 ),
 .UNSPECIFIED. ) ;
#17852=CARTESIAN_POINT ( 'NONE',  ( -86.55620429048337883, -23.47593901973091235, -1.443836447539002865 ) ) ;
#17853=CARTESIAN_POINT ( 'NONE',  ( -9.620199658202244208, 18.81650055922726494, 11.49999999999999645 ) ) ;
#17854=CARTESIAN_POINT ( 'NONE',  ( 22.09269804725545683, -1.632937629565654580, -1.500000000000002220 ) ) ;
#17855=CARTESIAN_POINT ( 'NONE',  ( -18.11865614447288664, 9.752654332028551920, 11.49999999999998934 ) ) ;
#17859=CARTESIAN_POINT ( 'NONE',  ( -54.50229491303872464, -24.15543982623906416, -0.2315651400026691176 ) ) ;
#17861=VERTEX_POINT ( 'NONE', #35442 ) ;
#17862=ORIENTED_EDGE ( 'NONE', *, *, #49822, .T. ) ;
#17863=ORIENTED_EDGE ( 'NONE', *, *, #82532, .T. ) ;
#17864=CARTESIAN_POINT ( 'NONE',  ( -81.62287095715008434, -24.33927499327855060, 9.819080762295817166 ) ) ;
#17867=CARTESIAN_POINT ( 'NONE',  ( -13.38394104848841693, -15.81244124602197765, -1.500000000000002220 ) ) ;
#17868=CARTESIAN_POINT ( 'NONE',  ( -6.994818212361641585, 20.52682044044541598, 11.49999999999999645 ) ) ;
#17869=ORIENTED_EDGE ( 'NONE', *, *, #11527, .T. ) ;
#17871=LINE ( 'NONE', #86873, #30228 ) ;
#17872=CARTESIAN_POINT ( 'NONE',  ( 15.70178742502441693, -15.98865493379879332, 11.49999999999998934 ) ) ;
#17873=CARTESIAN_POINT ( 'NONE',  ( -79.35008398046767297, -25.27874868537385922, 6.078937478087434343 ) ) ;
#17874=CARTESIAN_POINT ( 'NONE',  ( -58.52287095715006160, -23.47596703998600631, 11.44779298504228926 ) ) ;
#17875=EDGE_CURVE ( 'NONE', #29613, #60506, #41298, .T. ) ;
#17877=CARTESIAN_POINT ( 'NONE',  ( -45.62287095715004881, -24.99132157543083821, 2.256160258750667502 ) ) ;
#17878=CARTESIAN_POINT ( 'NONE',  ( -35.63736055960579563, -24.63419186844611986, 9.035850630976925757 ) ) ;
#17879=VERTEX_POINT ( 'NONE', #44546 ) ;
#17880=ORIENTED_EDGE ( 'NONE', *, *, #36432, .T. ) ;
#17883=CARTESIAN_POINT ( 'NONE',  ( -39.52287095715006870, -24.66019654487198665, 8.947790411086131712 ) ) ;
#17885=EDGE_CURVE ( 'NONE', #72803, #53441, #58285, .T. ) ;
#17886=PLANE ( 'NONE',  #74655 ) ;
#17887=CARTESIAN_POINT ( 'NONE',  ( -1.624102159174229731, 21.17438964843747584, -1.500000000000002220 ) ) ;
#17889=CARTESIAN_POINT ( 'NONE',  ( -88.51806581271243601, -23.73766607897670156, -1.055555164236456678 ) ) ;
#17890=CARTESIAN_POINT ( 'NONE',  ( -11.04117723084791614, -18.81814233335528286, 11.49999999999998934 ) ) ;
#17891=CARTESIAN_POINT ( 'NONE',  ( -103.6235449969178859, -24.66019654487200086, 8.947790411086119278 ) ) ;
#17892=B_SPLINE_CURVE_WITH_KNOTS ( 'NONE', 3,
 ( #59536, #98068, #12838, #66674, #5238, #60041, #36688, #50929, #51922, #90970, #5733, #82852, #51424, #28576, #58540, #97584, #13335, #44315 ),
 .UNSPECIFIED., .F., .F.,
 ( 4, 2, 2, 2, 2, 2, 2, 2, 4 ),
 ( 0.000000000000000000, 0.0002166463785664153835, 0.0004332927571328307670, 0.0008665855142656615339, 0.001083231892832076104, 0.001299878271398490675, 0.001733171028531327621, 0.002599756542797003901, 0.003466342057062679963 ),
 .UNSPECIFIED. ) ;
#17893=DIRECTION ( 'NONE',  ( 0.000000000000000000, 2.173523156925980399E-06, -0.9999999999976378895 ) ) ;
#17894=CARTESIAN_POINT ( 'NONE',  ( -50.52287095715006160, -24.99156044556120193, 7.747789690856173195 ) ) ;
#17895=CARTESIAN_POINT ( 'NONE',  ( -15.13543854793762300, 15.80457324685279374, -1.500000000000002220 ) ) ;
#17898=CARTESIAN_POINT ( 'NONE',  ( -65.62287095715007013, -24.15431212366392089, -0.2830839119429129358 ) ) ;
#17899=CARTESIAN_POINT ( 'NONE',  ( -85.62651978001045450, -24.83644354573578994, 8.397322867130101898 ) ) ;
#17903=ORIENTED_EDGE ( 'NONE', *, *, #72460, .F. ) ;
#17904=CARTESIAN_POINT ( 'NONE',  ( -28.88940304597720399, -25.00679290501443219, 2.971342454648660425 ) ) ;
#17907=CARTESIAN_POINT ( 'NONE',  ( -20.82729772986975547, -4.079710536234080642, -1.500000000000002220 ) ) ;
#17909=PLANE ( 'NONE',  #57637 ) ;
#17912=CARTESIAN_POINT ( 'NONE',  ( -68.62287095715005592, -29.50248528299804818, 1.056150453629036701 ) ) ;
#17913=EDGE_CURVE ( 'NONE', #24333, #81001, #36926, .T. ) ;
#17915=CARTESIAN_POINT ( 'NONE',  ( -8.724563080612403709, -17.33930400145671413, 11.49999999999998934 ) ) ;
#17917=VERTEX_POINT ( 'NONE', #13077 ) ;
#17918=CARTESIAN_POINT ( 'NONE',  ( 9.662506626059768067, -16.94115208737379774, 11.49999999999999645 ) ) ;
#17920=DIRECTION ( 'NONE',  ( -3.773278334453080206E-23, 0.9999999999976377785, 2.173523156925979975E-06 ) ) ;
#17923=EDGE_CURVE ( 'NONE', #82726, #90388, #47226, .T. ) ;
#17926=CARTESIAN_POINT ( 'NONE',  ( -88.52287095715006160, -23.47593901973090524, -1.443836447538996426 ) ) ;
#17927=CARTESIAN_POINT ( 'NONE',  ( -81.43785252974821276, -25.24813914738149734, 7.210847438489675021 ) ) ;
#17928=CARTESIAN_POINT ( 'NONE',  ( 16.09843989366402539, -11.26760994518913428, -1.500000000000002220 ) ) ;
#17930=DIRECTION ( 'NONE',  ( -3.773278334453079618E-23, 0.9999999999976377785, 2.173523156925979975E-06 ) ) ;
#17931=CARTESIAN_POINT ( 'NONE',  ( 21.75596283627254479, -7.788036635067100200, -1.500000000000002220 ) ) ;
#17935=CARTESIAN_POINT ( 'NONE',  ( -115.6228709571500843, -24.52323809116982645, 9.355190652339407720 ) ) ;
#17936=CARTESIAN_POINT ( 'NONE',  ( -29.52287095715007226, -23.86488628232234888, 10.65372853282540433 ) ) ;
#17937=CARTESIAN_POINT ( 'NONE',  ( -81.90384961113220186, -25.20144873054373136, 6.835696071488102099 ) ) ;
#17939=CARTESIAN_POINT ( 'NONE',  ( -73.52287095715011844, -24.51387760970724372, 9.387446482453396968 ) ) ;
#17940=CARTESIAN_POINT ( 'NONE',  ( -114.5946007866755281, -23.48786465467241769, 11.44779295918253759 ) ) ;
#17941=CARTESIAN_POINT ( 'NONE',  ( -18.10700488460823721, -8.296952762055457953, -1.500000000000002220 ) ) ;
#17942=EDGE_CURVE ( 'NONE', #17028, #7900, #28819, .T. ) ;
#17943=PLANE ( 'NONE',  #80854 ) ;
#17944=CARTESIAN_POINT ( 'NONE',  ( 19.87125486832220744, 0.9792442318621276121, -1.500000000000002220 ) ) ;
#17945=ORIENTED_EDGE ( 'NONE', *, *, #11965, .T. ) ;
#17947=CARTESIAN_POINT ( 'NONE',  ( -55.52287095715005449, -24.99132157543083821, 2.256160258750667502 ) ) ;
#17948=CARTESIAN_POINT ( 'NONE',  ( -35.62287095715005592, -24.99156045073392463, 7.747789690856161648 ) ) ;
#17949=CARTESIAN_POINT ( 'NONE',  ( -2.100290975465340271, -20.70549805216813510, 11.49999999999999645 ) ) ;
#17951=AXIS2_PLACEMENT_3D ( 'NONE', #41228, #47838, #80282 ) ;
#17952=EDGE_CURVE ( 'NONE', #55213, #4924, #15762, .T. ) ;
#17953=CARTESIAN_POINT ( 'NONE',  ( -126.6228709571500559, -24.64898659630529565, 1.056161002820834804 ) ) ;
#17954=CARTESIAN_POINT ( 'NONE',  ( 21.74077840044056842, -6.890983112422549794, 11.49999999999999645 ) ) ;
#17956=CARTESIAN_POINT ( 'NONE',  ( -76.52287095715007581, -29.50250243563736774, 8.947779886222141599 ) ) ;
#17957=EDGE_CURVE ( 'NONE', #79287, #56311, #36441, .T. ) ;
#17958=CARTESIAN_POINT ( 'NONE',  ( -41.62287095715006302, -29.50248528299804818, 1.056150453629031594 ) ) ;
#17960=CARTESIAN_POINT ( 'NONE',  ( 8.473373031455752269, -18.34320851062214430, -1.500000000000002220 ) ) ;
#17962=EDGE_CURVE ( 'NONE', #46989, #72780, #2487, .T. ) ;
#17966=ORIENTED_EDGE ( 'NONE', *, *, #5788, .F. ) ;
#17967=CARTESIAN_POINT ( 'NONE',  ( -20.47705334459679705, -22.77463087841388045, 11.50200000000000422 ) ) ;
#17968=CARTESIAN_POINT ( 'NONE',  ( -104.5228709571500758, -23.47596703998600631, 11.44779298504228215 ) ) ;
#17970=CARTESIAN_POINT ( 'NONE',  ( -1.591348192139008466, -19.94584644712825039, -1.500000000000002220 ) ) ;
#17971=CARTESIAN_POINT ( 'NONE',  ( 18.89479412359299815, 9.153864009170110450, 11.49999999999999645 ) ) ;
#17972=CARTESIAN_POINT ( 'NONE',  ( -28.16800187962948598, -24.70123718975396798, 8.197761918552000537 ) ) ;
#17973=CARTESIAN_POINT ( 'NONE',  ( -124.5194960560089612, -24.65952944569305316, 1.056160979905707009 ) ) ;
#17974=CARTESIAN_POINT ( 'NONE',  ( 21.54648482299927181, -4.703075207800759827, 11.49999999999998934 ) ) ;
#17975=CARTESIAN_POINT ( 'NONE',  ( -53.62287095715005592, -24.64965695001467694, 8.947790433994185832 ) ) ;
#17978=CARTESIAN_POINT ( 'NONE',  ( -49.52164473449563076, -25.18440224513725667, 3.857971350860132986 ) ) ;
#17979=CARTESIAN_POINT ( 'NONE',  ( -72.63498201661158760, -24.15543982623907127, -0.2315651400026661755 ) ) ;
#17984=CARTESIAN_POINT ( 'NONE',  ( -80.62287095715005592, -29.50248789122583659, 2.256150453626215580 ) ) ;
#17985=DIRECTION ( 'NONE',  ( -3.773278334453079030E-23, 0.9999999999976377785, 2.173523156925979128E-06 ) ) ;
#17986=CARTESIAN_POINT ( 'NONE',  ( -122.5562042904834215, -23.48786465467241769, 11.44779295918253759 ) ) ;
#17987=CARTESIAN_POINT ( 'NONE',  ( -5.951451697817415010, -19.63005813332872762, -1.500000000000002220 ) ) ;
#17991=CARTESIAN_POINT ( 'NONE',  ( -114.5228709571500616, -29.50250243563736774, 8.947779886222136270 ) ) ;
#17992=CARTESIAN_POINT ( 'NONE',  ( -15.13915969582853549, -16.40262476207453801, -1.500000000000002220 ) ) ;
#17993=CARTESIAN_POINT ( 'NONE',  ( -101.5228709571500758, -24.64965694238407323, 8.947790433994194714 ) ) ;
#17994=LINE ( 'NONE', #33723, #75624 ) ;
#17997=CARTESIAN_POINT ( 'NONE',  ( -43.55620429048338593, -24.65952944569304606, 1.056160979905693020 ) ) ;
#17999=CARTESIAN_POINT ( 'NONE',  ( 20.80141654084381386, -1.409215765453083469, 11.49999999999998934 ) ) ;
#18001=CARTESIAN_POINT ( 'NONE',  ( -112.5228709571500616, -24.64965694238408034, 8.947790433994192938 ) ) ;
#18002=EDGE_LOOP ( 'NONE', ( #74390, #15510, #92244, #49321 ) ) ;
#18003=ORIENTED_EDGE ( 'NONE', *, *, #94827, .T. ) ;
#18004=CARTESIAN_POINT ( 'NONE',  ( -68.94101663640660149, -25.25935064844479783, 6.247842340801990524 ) ) ;
#18005=CARTESIAN_POINT ( 'NONE',  ( 15.37114825158464271, 14.37155165002682544, -1.500000000000002220 ) ) ;
#18006=EDGE_LOOP ( 'NONE', ( #64819, #65851, #52673, #63825 ) ) ;
#18007=CARTESIAN_POINT ( 'NONE',  ( -89.52287095715006160, -29.50250786944525672, 11.44777988621623344 ) ) ;
#18010=CARTESIAN_POINT ( 'NONE',  ( -100.8646123533485621, -25.03152439226099091, 7.517421852973264151 ) ) ;
#18011=CARTESIAN_POINT ( 'NONE',  ( -73.62287095715005592, -24.65952944569304606, 1.056160979905698794 ) ) ;
#18012=CARTESIAN_POINT ( 'NONE',  ( 4.495418090846292181, 21.21921847905042569, -1.500000000000002220 ) ) ;
#18014=CARTESIAN_POINT ( 'NONE',  ( -17.34812393562427246, -13.96779696820907191, 11.49999999999999645 ) ) ;
#18016=CARTESIAN_POINT ( 'NONE',  ( -50.92793838057655620, -25.31441747217130001, 5.312585239957233973 ) ) ;
#18017=B_SPLINE_CURVE_WITH_KNOTS ( 'NONE', 3,
 ( #65122, #96042, #97040, #67110, #80317, #98019 ),
 .UNSPECIFIED., .F., .F.,
 ( 4, 2, 4 ),
 ( 6.384118678617895067E-06, 0.001386860460828379972, 0.002767336802978142326 ),
 .UNSPECIFIED. ) ;
#18018=CARTESIAN_POINT ( 'NONE',  ( -54.55620429048339304, -24.64898659630528499, 1.056161002820821260 ) ) ;
#18020=LINE ( 'NONE', #72319, #94397 ) ;
#18021=ORIENTED_EDGE ( 'NONE', *, *, #31712, .T. ) ;
#18024=EDGE_CURVE ( 'NONE', #49490, #89148, #33932, .T. ) ;
#18025=CARTESIAN_POINT ( 'NONE',  ( 11.25103634530202790, -16.72154935384561725, 11.49999999999998934 ) ) ;
#18028=CARTESIAN_POINT ( 'NONE',  ( -130.5728709571500588, -24.36716509058404156, 9.983964055416601369 ) ) ;
#18029=CARTESIAN_POINT ( 'NONE',  ( 22.03792223356247604, -4.036589945906135846, -1.500000000000002220 ) ) ;
#18030=VERTEX_POINT ( 'NONE', #91699 ) ;
#18031=ORIENTED_EDGE ( 'NONE', *, *, #53126, .F. ) ;
#18032=CARTESIAN_POINT ( 'NONE',  ( -112.5515187183059425, -24.51419770103158413, 9.386484678747166299 ) ) ;
#18033=CARTESIAN_POINT ( 'NONE',  ( -101.5957436026087635, -23.73791477778911485, 11.05961554403170233 ) ) ;
#18036=ADVANCED_FACE ( 'NONE', ( #7465 ), #4578, .T. ) ;
#18037=CARTESIAN_POINT ( 'NONE',  ( -41.52287095715004739, -23.73907113217657283, -1.053371485781501526 ) ) ;
#18038=EDGE_CURVE ( 'NONE', #76361, #1269, #35189, .T. ) ;
#18039=CARTESIAN_POINT ( 'NONE',  ( -30.59162032554853639, -24.82935162629096482, 1.633150109380538950 ) ) ;
#18040=AXIS2_PLACEMENT_3D ( 'NONE', #65749, #9934, #79946 ) ;
#18041=CARTESIAN_POINT ( 'NONE',  ( -6.824658503225996320, 18.35159230250476270, 11.49999999999998934 ) ) ;
#18042=CARTESIAN_POINT ( 'NONE',  ( -46.55319784584757770, -23.96119346886880308, -0.6495511937832144644 ) ) ;
#18045=CARTESIAN_POINT ( 'NONE',  ( -0.8555947871142663974, 21.52075748220454798, -1.500000000000002220 ) ) ;
#18046=CARTESIAN_POINT ( 'NONE',  ( -128.5214471550031305, -24.51314013834317151, 0.6176544820404290537 ) ) ;
#18047=CARTESIAN_POINT ( 'NONE',  ( -114.5228709571500758, -23.94994826722565762, -0.6494450866342721396 ) ) ;
#18048=CARTESIAN_POINT ( 'NONE',  ( -101.7587321196599532, -25.26650786476337984, 3.907930402413430482 ) ) ;
#18049=DIRECTION ( 'NONE',  ( -3.773278334453079030E-23, 0.9999999999976377785, 2.173523156925979128E-06 ) ) ;
#18050=CARTESIAN_POINT ( 'NONE',  ( 11.31314246093949727, 19.96360691973900359, -1.500000000000002220 ) ) ;
#18052=CARTESIAN_POINT ( 'NONE',  ( -93.62287095715008434, -24.34917612406837861, 0.1852690917426652040 ) ) ;
#18053=CARTESIAN_POINT ( 'NONE',  ( -49.66058267289122341, -23.48783264082477018, -1.443836473390093911 ) ) ;
#18054=CARTESIAN_POINT ( 'NONE',  ( -11.36185547594953249, 16.55520930037988592, 11.49999999999999645 ) ) ;
#18056=DIRECTION ( 'NONE',  ( -3.773278334453079618E-23, 0.9999999999976377785, 2.173523156925979975E-06 ) ) ;
#18057=PLANE ( 'NONE',  #92753 ) ;
#18058=FACE_OUTER_BOUND ( 'NONE', #60120, .T. ) ;
#18060=CARTESIAN_POINT ( 'NONE',  ( 18.78741845327603599, -6.401996767227196905, -1.500000000000002220 ) ) ;
#18063=CARTESIAN_POINT ( 'NONE',  ( -10.66912846187372210, -16.51573522771486324, -1.500000000000002220 ) ) ;
#18065=EDGE_CURVE ( 'NONE', #92149, #40482, #6063, .T. ) ;
#18066=CARTESIAN_POINT ( 'NONE',  ( -58.55620429048339304, -23.48786465467241058, 11.44779295918254469 ) ) ;
#18068=CARTESIAN_POINT ( 'NONE',  ( -57.52287095715003318, -23.95044443724990657, 10.65354141964648882 ) ) ;
#18070=CARTESIAN_POINT ( 'NONE',  ( 6.296002175621457475, 19.65409743616946514, 11.49999999999999645 ) ) ;
#18072=ADVANCED_FACE ( 'NONE', ( #9475 ), #1871, .T. ) ;
#18073=CARTESIAN_POINT ( 'NONE',  ( -120.5877768927123412, -25.00158670708911046, 2.256160236439219258 ) ) ;
#18074=CARTESIAN_POINT ( 'NONE',  ( -14.16962031475959272, 17.58799634409329471, 11.49999999999999645 ) ) ;
#18076=ORIENTED_EDGE ( 'NONE', *, *, #25593, .F. ) ;
#18077=CARTESIAN_POINT ( 'NONE',  ( -69.38174606678134637, -25.25639464550703295, 6.471609011167150705 ) ) ;
#18078=DIRECTION ( 'NONE',  ( 1.000000000000000000, 3.773278334444166432E-23, 8.201307841325785021E-29 ) ) ;
#18080=CARTESIAN_POINT ( 'NONE',  ( -39.62287095715004170, -23.94994826722515313, -0.6494450866351729745 ) ) ;
#18081=B_SPLINE_CURVE_WITH_KNOTS ( 'NONE', 3,
 ( #94378, #9646, #2050, #78134 ),
 .UNSPECIFIED., .F., .F.,
 ( 4, 4 ),
 ( 0.000000000000000000, 9.999999999998897304E-05 ),
 .UNSPECIFIED. ) ;
#18082=CARTESIAN_POINT ( 'NONE',  ( -26.59548113855183615, -24.93063557578396328, 7.895922241538460895 ) ) ;
#18083=EDGE_CURVE ( 'NONE', #36438, #34988, #53345, .T. ) ;
#18084=CARTESIAN_POINT ( 'NONE',  ( -75.58953762381673869, -23.47593901973091235, -1.443836447539004642 ) ) ;
#18087=CARTESIAN_POINT ( 'NONE',  ( -80.43221577628075636, -25.26749876250476490, 4.967019860322055891 ) ) ;
#18088=CARTESIAN_POINT ( 'NONE',  ( -22.57016884136470125, -3.422276288085174478, -1.500000000000002220 ) ) ;
#18089=CARTESIAN_POINT ( 'NONE',  ( -74.49656298872699267, -24.65952944569304606, 1.056160979905701902 ) ) ;
#18090=EDGE_CURVE ( 'NONE', #27395, #38340, #56674, .T. ) ;
#18091=CARTESIAN_POINT ( 'NONE',  ( -122.6228709571500417, -29.50250786944525672, 11.44777988621622811 ) ) ;
#18092=FACE_OUTER_BOUND ( 'NONE', #27702, .T. ) ;
#18093=CARTESIAN_POINT ( 'NONE',  ( -19.72384299526936857, -10.77339039931002773, 11.49999999999999645 ) ) ;
#18094=ORIENTED_EDGE ( 'NONE', *, *, #57130, .F. ) ;
#18096=VECTOR ( 'NONE', #16046, 1000.000000000000114 ) ;
#18097=CARTESIAN_POINT ( 'NONE',  ( -21.97012646571106842, -0.5360883523215664859, 11.49999999999998934 ) ) ;
#18098=CARTESIAN_POINT ( 'NONE',  ( -54.62287095715007723, -24.34917612406837861, 0.1852690917426598194 ) ) ;
#18099=CARTESIAN_POINT ( 'NONE',  ( -34.52200844785745204, -23.48786465467240347, 11.44779295918255535 ) ) ;
#18100=FACE_OUTER_BOUND ( 'NONE', #62262, .T. ) ;
#18101=VERTEX_POINT ( 'NONE', #10473 ) ;
#18102=CARTESIAN_POINT ( 'NONE',  ( -51.70072539166535108, -25.27314792116673203, 3.987152059579775809 ) ) ;
#18103=DIRECTION ( 'NONE',  ( 1.000000000000000000, 3.773278334444167608E-23, 8.201307833595939069E-29 ) ) ;
#18104=ORIENTED_EDGE ( 'NONE', *, *, #22488, .F. ) ;
#18105=CARTESIAN_POINT ( 'NONE',  ( -54.53711127335206044, -24.51419770103157347, 9.386484678747178734 ) ) ;
#18106=CARTESIAN_POINT ( 'NONE',  ( 16.11427877760282001, 12.65940972936023812, 11.49999999999998934 ) ) ;
#18108=EDGE_LOOP ( 'NONE', ( #6266, #50302, #60210, #79753 ) ) ;
#18109=ORIENTED_EDGE ( 'NONE', *, *, #24836, .T. ) ;
#18110=VERTEX_POINT ( 'NONE', #41431 ) ;
#18112=CARTESIAN_POINT ( 'NONE',  ( -84.62287095715004170, -24.34917612406837861, 0.1852690917426652040 ) ) ;
#18113=CARTESIAN_POINT ( 'NONE',  ( 11.75533340255842596, 19.88161105567325038, -1.500000000000002220 ) ) ;
#18114=CARTESIAN_POINT ( 'NONE',  ( -104.6250114612373494, -24.51419770103158768, 9.386484678747164523 ) ) ;
#18115=CARTESIAN_POINT ( 'NONE',  ( -16.75749313124890350, -11.57646860041911019, -1.500000000000002220 ) ) ;
#18120=CARTESIAN_POINT ( 'NONE',  ( -70.48669981260067630, -25.00158670708910691, 2.256160236439221034 ) ) ;
#18122=FACE_OUTER_BOUND ( 'NONE', #1288, .T. ) ;
#18123=CARTESIAN_POINT ( 'NONE',  ( -49.11003834631243592, -25.26385671119021836, 4.144493137612085043 ) ) ;
#18125=EDGE_LOOP ( 'NONE', ( #36737, #94143, #9761, #69540 ) ) ;
#18126=CARTESIAN_POINT ( 'NONE',  ( -18.04518632387085830, 10.29925911722504317, -1.500000000000002220 ) ) ;
#18128=CARTESIAN_POINT ( 'NONE',  ( -91.52287095715006160, -24.64898659630368272, 1.056161002820827921 ) ) ;
#18129=ORIENTED_EDGE ( 'NONE', *, *, #64581, .T. ) ;
#18131=CARTESIAN_POINT ( 'NONE',  ( -40.62287095715004170, -25.00158670708908204, 2.256160236439166411 ) ) ;
#18132=VERTEX_POINT ( 'NONE', #33815 ) ;
#18135=CARTESIAN_POINT ( 'NONE',  ( -127.6228709571500559, -29.50250786944525672, 11.44777988621622633 ) ) ;
#18137=CARTESIAN_POINT ( 'NONE',  ( -22.07534667767119174, -0.2742745133902674826, 11.49999999999999645 ) ) ;
#18139=CARTESIAN_POINT ( 'NONE',  ( -48.87575205656965238, -25.25459236073634983, 6.222261992663564278 ) ) ;
#18140=CARTESIAN_POINT ( 'NONE',  ( -20.50338545487000275, 9.463669735852004550, 11.49999999999998934 ) ) ;
#18141=CARTESIAN_POINT ( 'NONE',  ( -70.62287095715005592, -23.47593901973091235, -1.443836447539006196 ) ) ;
#18142=ORIENTED_EDGE ( 'NONE', *, *, #91154, .T. ) ;
#18143=ORIENTED_EDGE ( 'NONE', *, *, #8547, .T. ) ;
#18144=CARTESIAN_POINT ( 'NONE',  ( -88.52287095715010423, -24.51387760970724727, 9.387446482453404073 ) ) ;
#18146=DIRECTION ( 'NONE',  ( -3.773278334453079030E-23, 0.9999999999976377785, 2.173523156925979128E-06 ) ) ;
#18147=VERTEX_POINT ( 'NONE', #95716 ) ;
#18148=CARTESIAN_POINT ( 'NONE',  ( -0.1268723920767304558, 21.18662008908366445, 11.49999999999998934 ) ) ;
#18149=CARTESIAN_POINT ( 'NONE',  ( -34.62287095715003460, -23.73934037231755667, 11.05740245334329508 ) ) ;
#18153=DIRECTION ( 'NONE',  ( -1.000000000000000000, -3.773278334444167608E-23, -8.201307833595939069E-29 ) ) ;
#18154=CARTESIAN_POINT ( 'NONE',  ( -15.91109736606077441, 15.52988587838853540, -1.500000000000002220 ) ) ;
#18156=CARTESIAN_POINT ( 'NONE',  ( -114.5180551983652322, -24.15543982623907837, -0.2315651400026444429 ) ) ;
#18157=ADVANCED_FACE ( 'NONE', ( #10980 ), #33684, .T. ) ;
#18158=ORIENTED_EDGE ( 'NONE', *, *, #81844, .T. ) ;
#18159=CARTESIAN_POINT ( 'NONE',  ( -112.5228709571500474, -24.51283580621457858, 0.6167428607047616973 ) ) ;
#18161=CARTESIAN_POINT ( 'NONE',  ( 11.20917403917954225, 15.81763734437701885, 11.49999999999999645 ) ) ;
#18162=ADVANCED_FACE ( 'NONE', ( #12961 ), #50541, .F. ) ;
#18165=CARTESIAN_POINT ( 'NONE',  ( -77.62287095715005592, -23.47593901973091235, -1.443836447539004642 ) ) ;
#18166=CARTESIAN_POINT ( 'NONE',  ( 16.53150372360616771, 10.32350692489952593, 11.49999999999998934 ) ) ;
#18167=CARTESIAN_POINT ( 'NONE',  ( 21.39645853268639186, 0.3907444525687319703, 11.49999999999998934 ) ) ;
#18168=CARTESIAN_POINT ( 'NONE',  ( -62.52287095715006160, -23.47596703998600631, 11.44779298504228926 ) ) ;
#18171=DIRECTION ( 'NONE',  ( -3.773278334453079618E-23, 0.9999999999976377785, 2.173523156925979975E-06 ) ) ;
#18172=CARTESIAN_POINT ( 'NONE',  ( -77.50095171770020386, -24.51314013834315375, 0.6176544820404117342 ) ) ;
#18173=CARTESIAN_POINT ( 'NONE',  ( 6.135622925040504327, -21.92205258971886650, -1.500000000000002220 ) ) ;
#18175=CARTESIAN_POINT ( 'NONE',  ( -102.5855002951087585, -24.65952944569305316, 1.056160979905705677 ) ) ;
#18176=CARTESIAN_POINT ( 'NONE',  ( -127.6228709571500559, -23.48783264082479505, -1.443836473390056829 ) ) ;
#18177=CARTESIAN_POINT ( 'NONE',  ( 10.08953278062578462, 17.19620541797624824, 11.49999999999999645 ) ) ;
#18178=CARTESIAN_POINT ( 'NONE',  ( -31.52287095715006160, -23.47593901973090169, -1.443836447538997536 ) ) ;
#18179=CARTESIAN_POINT ( 'NONE',  ( -39.63465047039538547, -24.35071581493543036, 9.817618358456035921 ) ) ;
#18182=PLANE ( 'NONE',  #31500 ) ;
#18184=CARTESIAN_POINT ( 'NONE',  ( -77.52287095715007581, -24.51283580621364422, 0.6167428607019788123 ) ) ;
#18186=CARTESIAN_POINT ( 'NONE',  ( -17.90551237062050305, -12.20792721910736667, 11.49999999999998934 ) ) ;
#18187=CARTESIAN_POINT ( 'NONE',  ( -35.52287095715006870, -29.50250243563736774, 8.947779886222148704 ) ) ;
#18188=CARTESIAN_POINT ( 'NONE',  ( 12.63578256557813795, 14.83599306707809085, -1.500000000000002220 ) ) ;
#18189=CARTESIAN_POINT ( 'NONE',  ( -93.52287095715010423, -24.34917612406837861, 0.1852690917426536021 ) ) ;
#18194=CARTESIAN_POINT ( 'NONE',  ( -86.62287095715004170, -29.50247984919015209, -1.443849546365051806 ) ) ;
#18195=CARTESIAN_POINT ( 'NONE',  ( 5.028806042385554953, -19.83023610923392610, 11.49999999999999645 ) ) ;
#18199=CARTESIAN_POINT ( 'NONE',  ( -72.52287095715007581, -23.96127896941631619, -0.6493128931038039120 ) ) ;
#18201=CARTESIAN_POINT ( 'NONE',  ( -39.04762117679405264, -25.31628479640222906, 4.358277408297509758 ) ) ;
#18202=B_SPLINE_CURVE_WITH_KNOTS ( 'NONE', 3,
 ( #51575, #36848, #28229, #13988 ),
 .UNSPECIFIED., .F., .F.,
 ( 4, 4 ),
 ( 0.3007147330300765087, 0.3097211643021920424 ),
 .UNSPECIFIED. ) ;
#18203=CARTESIAN_POINT ( 'NONE',  ( -110.6228709571500559, -29.50247984919015209, -1.443849546365048253 ) ) ;
#18205=CARTESIAN_POINT ( 'NONE',  ( -109.5151497621329213, -24.34968618360934300, 0.1864209137778879422 ) ) ;
#18207=CARTESIAN_POINT ( 'NONE',  ( -66.51027937953499247, -23.96169478059713143, 10.65365249895718058 ) ) ;
#18209=CARTESIAN_POINT ( 'NONE',  ( 3.929728083993185184, -22.62717521373229701, 11.49999999999999645 ) ) ;
#18210=CARTESIAN_POINT ( 'NONE',  ( 18.68554041145753786, -12.99315341008173519, -1.500000000000002220 ) ) ;
#18211=CARTESIAN_POINT ( 'NONE',  ( -110.6241301225872888, -24.92592662359561828, 8.075495903018000021 ) ) ;
#18212=B_SPLINE_SURFACE_WITH_KNOTS ( 'NONE', 3, 3, ( 
 ( #47748, #17287, #33021, #78167 ),
 ( #61972, #16283, #92899, #31006 ),
 ( #39621, #63996, #48251, #47243 ),
 ( #23376, #70072, #8681, #40638 ) ),
 .UNSPECIFIED., .F., .F., .F.,
 ( 4, 4 ),
 ( 4, 4 ),
 ( 0.5218268152168922258, 0.6546831510031384527 ),
 ( 0.5925805111453674723, 0.6124317898845940134 ),
 .UNSPECIFIED. ) ;
#18214=CARTESIAN_POINT ( 'NONE',  ( -113.6228709571500559, -24.65952944569304961, 1.056160979905706565 ) ) ;
#18216=CARTESIAN_POINT ( 'NONE',  ( -82.62287095715005592, -23.48783264082478084, -1.443836473390065933 ) ) ;
#18217=EDGE_CURVE ( 'NONE', #98343, #47218, #57665, .T. ) ;
#18218=CARTESIAN_POINT ( 'NONE',  ( -1.606994170628035068, 21.82944698466814870, 11.49999999999998934 ) ) ;
#18221=CARTESIAN_POINT ( 'NONE',  ( -115.6228709571500417, -23.85196035786902513, -0.8779234886474898136 ) ) ;
#18222=PLANE ( 'NONE',  #32250 ) ;
#18224=ORIENTED_EDGE ( 'NONE', *, *, #61337, .T. ) ;
#18226=CARTESIAN_POINT ( 'NONE',  ( -16.87313589883980214, -11.49665204554024989, 11.49999999999998934 ) ) ;
#18229=CARTESIAN_POINT ( 'NONE',  ( 10.47623847176155820, -20.49086732513842080, 11.49999999999998934 ) ) ;
#18231=VERTEX_POINT ( 'NONE', #58164 ) ;
#18232=CARTESIAN_POINT ( 'NONE',  ( -32.52287095715006160, -29.50248528299804818, 1.056150453629029817 ) ) ;
#18233=CARTESIAN_POINT ( 'NONE',  ( -50.22287095715005734, -23.47593901973090169, -1.443836447538997980 ) ) ;
#18234=LINE ( 'NONE', #11118, #38172 ) ;
#18235=CARTESIAN_POINT ( 'NONE',  ( -53.48691055854919085, -24.66019654487199375, 8.947790411086122830 ) ) ;
#18236=CARTESIAN_POINT ( 'NONE',  ( 20.74164082462262471, 5.259929546262127609, 11.49999999999999645 ) ) ;
#18239=EDGE_LOOP ( 'NONE', ( #96702, #99328, #11265, #78231 ) ) ;
#18240=CARTESIAN_POINT ( 'NONE',  ( -20.66209241242137296, -8.185968977665980972, 11.49999999999998934 ) ) ;
#18241=CARTESIAN_POINT ( 'NONE',  ( 7.914317726235799100, 19.11507755054979896, -1.500000000000002220 ) ) ;
#18245=ORIENTED_EDGE ( 'NONE', *, *, #89441, .T. ) ;
#18246=DIRECTION ( 'NONE',  ( 0.000000000000000000, -0.9999999999976377785, -2.173523156925979975E-06 ) ) ;
#18247=ORIENTED_EDGE ( 'NONE', *, *, #25756, .F. ) ;
#18248=CARTESIAN_POINT ( 'NONE',  ( -91.52287095715006160, -24.64898659630368272, 1.056161002820827921 ) ) ;
#18249=CARTESIAN_POINT ( 'NONE',  ( -70.32380231474228083, -25.12298712672050982, 7.101635559041870494 ) ) ;
#18250=CARTESIAN_POINT ( 'NONE',  ( 20.36350155627077640, -4.707376482769925374, -1.500000000000002220 ) ) ;
#18251=CARTESIAN_POINT ( 'NONE',  ( 13.86046232669119149, 16.88393516940953276, 11.49999999999999645 ) ) ;
#18253=FACE_OUTER_BOUND ( 'NONE', #19221, .T. ) ;
#18254=CARTESIAN_POINT ( 'NONE',  ( 22.09666729679958053, 4.251135690456572469, -1.500000000000002220 ) ) ;
#18255=CARTESIAN_POINT ( 'NONE',  ( -9.975069251262826953, -18.38325097723136992, -1.500000000000002220 ) ) ;
#18256=CARTESIAN_POINT ( 'NONE',  ( -26.10989220437014424, -24.97066886156136079, 5.384402865666523041 ) ) ;
#18257=CARTESIAN_POINT ( 'NONE',  ( -53.58953762381672448, -24.64898659630528499, 1.056161002820821704 ) ) ;
#18259=CARTESIAN_POINT ( 'NONE',  ( -31.24388727629347784, -24.87219037989215309, 1.747789950310770779 ) ) ;
#18262=ORIENTED_EDGE ( 'NONE', *, *, #19539, .T. ) ;
#18263=ORIENTED_EDGE ( 'NONE', *, *, #74378, .F. ) ;
#18264=CARTESIAN_POINT ( 'NONE',  ( -38.62287095715005592, -24.66019654487199020, 8.947790411086137041 ) ) ;
#18265=ORIENTED_EDGE ( 'NONE', *, *, #38909, .F. ) ;
#18266=CARTESIAN_POINT ( 'NONE',  ( 18.17913347391500523, 11.28257676469832660, -1.500000000000002220 ) ) ;
#18267=VECTOR ( 'NONE', #29407, 1000.000000000000114 ) ;
#18268=CARTESIAN_POINT ( 'NONE',  ( 22.01400519847025450, -3.885951517071169370, 11.49999999999999645 ) ) ;
#18269=ORIENTED_EDGE ( 'NONE', *, *, #75986, .T. ) ;
#18271=CARTESIAN_POINT ( 'NONE',  ( -12.45680796028966597, 17.00782699154285638, 11.49999999999998934 ) ) ;
#18272=CARTESIAN_POINT ( 'NONE',  ( -30.57655019826978560, -25.31558489090919650, 5.002391647799127483 ) ) ;
#18273=ADVANCED_FACE ( 'NONE', ( #4377 ), #66286, .T. ) ;
#18276=CARTESIAN_POINT ( 'NONE',  ( -80.74930246458728789, -25.29534355928818457, 4.554285777995756845 ) ) ;
#18277=CARTESIAN_POINT ( 'NONE',  ( 13.08019894233326319, 17.74467248152726384, -1.500000000000002220 ) ) ;
#18278=EDGE_LOOP ( 'NONE', ( #54098, #72833, #45806, #73511 ) ) ;
#18279=CARTESIAN_POINT ( 'NONE',  ( -65.63042416189901473, -24.73531770709095312, 8.716586749053508498 ) ) ;
#18280=ADVANCED_FACE ( 'NONE', ( #53547 ), #67784, .T. ) ;
#18281=LINE ( 'NONE', #95405, #27106 ) ;
#18283=ADVANCED_FACE ( 'NONE', ( #84972 ), #45437, .T. ) ;
#18284=CARTESIAN_POINT ( 'NONE',  ( -29.85518128034571461, -24.80592719104361521, 8.290116722409051064 ) ) ;
#18285=EDGE_CURVE ( 'NONE', #20207, #87834, #29694, .T. ) ;
#18286=PLANE ( 'NONE',  #50569 ) ;
#18287=CARTESIAN_POINT ( 'NONE',  ( -38.62287095715004881, -24.35013146730202038, 9.818937971375113705 ) ) ;
#18288=CARTESIAN_POINT ( 'NONE',  ( 1.434216325579209750, -21.26356369375713484, 11.49999999999998934 ) ) ;
#18290=ADVANCED_FACE ( 'NONE', ( #21566 ), #22066, .T. ) ;
#18291=CARTESIAN_POINT ( 'NONE',  ( -117.5228709571501184, -24.35013146730205236, 9.818937971375092388 ) ) ;
#18292=CARTESIAN_POINT ( 'NONE',  ( -37.62287095715005592, -29.50250786944525672, 11.44777988621624232 ) ) ;
#18294=CARTESIAN_POINT ( 'NONE',  ( 21.27769986149581172, 7.469961712261545372, -1.500000000000002220 ) ) ;
#18296=B_SPLINE_SURFACE_WITH_KNOTS ( 'NONE', 3, 3, ( 
 ( #57307, #10602, #95341, #3008 ),
 ( #33945, #64925, #32949, #11102 ),
 ( #65918, #71518, #48179, #34447 ),
 ( #96341, #72020, #25828, #26332 ),
 ( #50175, #96835, #79109, #9604 ),
 ( #40566, #2503, #2002, #25326 ),
 ( #63922, #48689, #79612, #60788 ) ),
 .UNSPECIFIED., .F., .F., .F.,
 ( 4, 3, 4 ),
 ( 4, 4 ),
 ( 0.7945040050992244751, 0.8970133687736505657, 0.9995227324480766562 ),
 ( 0.6096489174824381019, 0.6109430964335138547 ),
 .UNSPECIFIED. ) ;
#18297=CARTESIAN_POINT ( 'NONE',  ( -89.40841769935769889, -25.23397913219577049, 6.409327625469732226 ) ) ;
#18299=CARTESIAN_POINT ( 'NONE',  ( -35.62287095715005592, -25.00182538069145011, 7.747789668545097541 ) ) ;
#18301=CARTESIAN_POINT ( 'NONE',  ( -9.297559507673007317, 17.40068379117045083, 11.49999999999999645 ) ) ;
#18303=CARTESIAN_POINT ( 'NONE',  ( -67.58779132469727813, -24.34968618360933235, 0.1864209137778811143 ) ) ;
#18304=EDGE_LOOP ( 'NONE', ( #23275, #29257, #65944, #44344 ) ) ;
#18306=LINE ( 'NONE', #32526, #91784 ) ;
#18308=CARTESIAN_POINT ( 'NONE',  ( -124.5202219396526857, -24.35071581493544457, 9.817618358456016381 ) ) ;
#18310=CARTESIAN_POINT ( 'NONE',  ( -120.5895376238167245, -24.99132157543166954, 2.256160258750667502 ) ) ;
#18311=EDGE_CURVE ( 'NONE', #40376, #24964, #60664, .T. ) ;
#18312=CARTESIAN_POINT ( 'NONE',  ( -68.52287095715006160, -24.64965694238407323, 8.947790433994200043 ) ) ;
#18313=CARTESIAN_POINT ( 'NONE',  ( 5.507670110241905448, 19.00313184189250038, -1.500000000000002220 ) ) ;
#18315=VECTOR ( 'NONE', #75326, 1000.000000000000114 ) ;
#18316=CARTESIAN_POINT ( 'NONE',  ( 13.23653054071972512, 15.24542462990338088, 11.49999999999999645 ) ) ;
#18319=CARTESIAN_POINT ( 'NONE',  ( -110.6228709571500985, -24.63287334234179937, 0.9662140553045460711 ) ) ;
#18320=CARTESIAN_POINT ( 'NONE',  ( -100.6814946224345846, -25.30267106336103922, 4.736250553104468963 ) ) ;
#18322=CARTESIAN_POINT ( 'NONE',  ( -122.5562042904833930, -23.47596703998600631, 11.44779298504227683 ) ) ;
#18323=CARTESIAN_POINT ( 'NONE',  ( -52.55620429048339304, -24.64898659630528144, 1.056161002820821038 ) ) ;
#18324=CARTESIAN_POINT ( 'NONE',  ( -96.52287095715006160, -24.65952944569304606, 1.056160979905702346 ) ) ;
#18325=CARTESIAN_POINT ( 'NONE',  ( 19.65109224456760728, -3.968444974485820786, -1.500000000000002220 ) ) ;
#18327=ORIENTED_EDGE ( 'NONE', *, *, #44409, .T. ) ;
#18330=CARTESIAN_POINT ( 'NONE',  ( -73.62287095715007013, -24.50321055353806088, 9.387540953477531147 ) ) ;
#18332=PLANE ( 'NONE',  #1430 ) ;
#18334=CARTESIAN_POINT ( 'NONE',  ( -101.7380495759637284, -25.24922313465046386, 3.830795054426443524 ) ) ;
#18338=CARTESIAN_POINT ( 'NONE',  ( -73.62287095715005592, -23.48783264082478084, -1.443836473390067487 ) ) ;
#18339=ORIENTED_EDGE ( 'NONE', *, *, #23929, .T. ) ;
#18340=CARTESIAN_POINT ( 'NONE',  ( -18.82647582233506611, 7.659846263794035437, 11.49999999999998934 ) ) ;
#18342=ORIENTED_EDGE ( 'NONE', *, *, #53679, .F. ) ;
#18344=CARTESIAN_POINT ( 'NONE',  ( -32.61958528550577086, -23.48783264082477729, -1.443836473390076147 ) ) ;
#18345=CARTESIAN_POINT ( 'NONE',  ( -127.5898610374712803, -24.15620529776628800, 10.23563542870658871 ) ) ;
#18347=CARTESIAN_POINT ( 'NONE',  ( -59.63756292401139802, -24.15620529776628445, 10.23563542870661180 ) ) ;
#18348=CARTESIAN_POINT ( 'NONE',  ( -50.28030459868799795, -25.12215419117113768, 7.099251938033546594 ) ) ;
#18349=CARTESIAN_POINT ( 'NONE',  ( -86.52287095715006160, -23.47593901973090169, -1.443836447538996648 ) ) ;
#18350=CARTESIAN_POINT ( 'NONE',  ( 18.68757921870947669, -9.911485057863893999, 11.49999999999999645 ) ) ;
#18351=CARTESIAN_POINT ( 'NONE',  ( 19.07224962250127831, -11.27678277851665634, -1.500000000000002220 ) ) ;
#18353=CARTESIAN_POINT ( 'NONE',  ( 11.93631617611541351, -16.73449621718459923, -1.500000000000002220 ) ) ;
#18355=CARTESIAN_POINT ( 'NONE',  ( -91.52287095715006160, -23.47596703998600631, 11.44779298504228393 ) ) ;
#18357=CARTESIAN_POINT ( 'NONE',  ( -116.6228709571500559, -29.50250243563736774, 8.947779886222134493 ) ) ;
#18358=DIRECTION ( 'NONE',  ( -3.773278334453079618E-23, 0.9999999999976377785, 2.173523156925979975E-06 ) ) ;
#18362=CARTESIAN_POINT ( 'NONE',  ( -70.52287095715007581, -23.48786465467241769, 11.44779295918254647 ) ) ;
#18364=CARTESIAN_POINT ( 'NONE',  ( -91.62287095715004170, -24.65952944569304606, 1.056160979905700792 ) ) ;
#18365=CARTESIAN_POINT ( 'NONE',  ( 13.32396043830641830, 15.83023408377254704, -1.500000000000002220 ) ) ;
#18366=CARTESIAN_POINT ( 'NONE',  ( 15.40532884848888884, -15.22192433072940609, 11.49999999999999645 ) ) ;
#18369=CARTESIAN_POINT ( 'NONE',  ( -60.52287095715003318, -24.52323809117613607, 9.355190652322249889 ) ) ;
#18371=CARTESIAN_POINT ( 'NONE',  ( -8.193370562272118462, -20.86776251599019361, 11.49999999999998934 ) ) ;
#18373=CARTESIAN_POINT ( 'NONE',  ( -71.62287095715005592, -24.65952944569304606, 1.056160979905699016 ) ) ;
#18375=CARTESIAN_POINT ( 'NONE',  ( -31.62287095715005236, -24.66019654487199020, 8.947790411086138818 ) ) ;
#18376=CARTESIAN_POINT ( 'NONE',  ( -89.40841769935767047, -25.05712065398430966, 7.447789548358837663 ) ) ;
#18378=VERTEX_POINT ( 'NONE', #91586 ) ;
#18379=ORIENTED_EDGE ( 'NONE', *, *, #6797, .F. ) ;
#18381=ORIENTED_EDGE ( 'NONE', *, *, #33550, .F. ) ;
#18382=B_SPLINE_CURVE_WITH_KNOTS ( 'NONE', 3,
 ( #51963, #59084, #90021, #81908, #82892, #12386 ),
 .UNSPECIFIED., .F., .F.,
 ( 4, 2, 4 ),
 ( 1.570887131794638196E-05, 0.001396322306279759555, 0.002776935741241572803 ),
 .UNSPECIFIED. ) ;
#18383=PLANE ( 'NONE',  #66586 ) ;
#18384=CARTESIAN_POINT ( 'NONE',  ( -9.361133326760958440, -19.03884994183470880, -1.500000000000002220 ) ) ;
#18385=EDGE_LOOP ( 'NONE', ( #93843, #77218, #35075, #38856 ) ) ;
#18386=CARTESIAN_POINT ( 'NONE',  ( -88.55459573829534747, -23.96119346886880308, -0.6495511937832096905 ) ) ;
#18387=CARTESIAN_POINT ( 'NONE',  ( 11.26692973276593968, -18.67385317477220497, 11.49999999999998934 ) ) ;
#18388=CARTESIAN_POINT ( 'NONE',  ( -52.53661446490540499, -24.51419770103158413, 9.386484678747187615 ) ) ;
#18389=CARTESIAN_POINT ( 'NONE',  ( -111.9545715455114987, -29.50249917535260380, 7.447779886225679213 ) ) ;
#18391=CARTESIAN_POINT ( 'NONE',  ( -19.96805355746080934, -8.928269573510897672, -1.500000000000002220 ) ) ;
#18392=CARTESIAN_POINT ( 'NONE',  ( -109.5228709571500616, -23.73934037231757443, 11.05740245334328087 ) ) ;
#18396=ORIENTED_EDGE ( 'NONE', *, *, #50954, .T. ) ;
#18398=CARTESIAN_POINT ( 'NONE',  ( -30.61271081598701471, -24.37855497370575009, 0.3021426168933804557 ) ) ;
#18399=EDGE_LOOP ( 'NONE', ( #70892, #91823, #8261, #96750 ) ) ;
#18401=LINE ( 'NONE', #49370, #56683 ) ;
#18402=CARTESIAN_POINT ( 'NONE',  ( -82.55439603937421111, -23.96119346886881019, -0.6495511937831923710 ) ) ;
#18403=CARTESIAN_POINT ( 'NONE',  ( 1.624102159173431259, 21.17561035156254334, 11.49999999999998934 ) ) ;
#18405=ADVANCED_FACE ( 'NONE', ( #76352 ), #63650, .T. ) ;
#18406=CARTESIAN_POINT ( 'NONE',  ( -30.62200344337180269, -24.13759587396041439, -0.5132947483565731828 ) ) ;
#18407=CARTESIAN_POINT ( 'NONE',  ( -67.52287095715006160, -29.50250243563736774, 8.947779886222143375 ) ) ;
#18408=CARTESIAN_POINT ( 'NONE',  ( -68.64584877695018861, -23.73766607897669445, -1.055555164236457788 ) ) ;
#18410=CARTESIAN_POINT ( 'NONE',  ( 1.664315604108443925, 19.36118569274438528, 11.49999999999998934 ) ) ;
#18411=CARTESIAN_POINT ( 'NONE',  ( -45.54237047602679667, -24.40034930558990922, 0.3402023900116019073 ) ) ;
#18412=EDGE_LOOP ( 'NONE', ( #56330, #77080, #48091, #35086 ) ) ;
#18413=CARTESIAN_POINT ( 'NONE',  ( 18.23270504744370868, -6.907985942191454676, 11.49999999999999645 ) ) ;
#18416=CARTESIAN_POINT ( 'NONE',  ( -42.58953762381671737, -23.48786465467240347, 11.44779295918255180 ) ) ;
#18417=EDGE_CURVE ( 'NONE', #20796, #97996, #90894, .T. ) ;
#18418=ORIENTED_EDGE ( 'NONE', *, *, #55648, .F. ) ;
#18419=DIRECTION ( 'NONE',  ( 0.000000000000000000, -0.9999999999976377785, -2.173523156925979128E-06 ) ) ;
#18420=CARTESIAN_POINT ( 'NONE',  ( -89.54842567568222478, -24.34968618360934300, 0.1864209137778942982 ) ) ;
#18421=CARTESIAN_POINT ( 'NONE',  ( -80.62287095715007013, -23.47596703998600631, 11.44779298504227860 ) ) ;
#18422=CARTESIAN_POINT ( 'NONE',  ( -81.88534077628074215, -25.03155785007460565, 6.293943450071303403 ) ) ;
#18423=CARTESIAN_POINT ( 'NONE',  ( 5.252985061998082017, 18.97096265210048571, 11.49999999999998934 ) ) ;
#18424=EDGE_LOOP ( 'NONE', ( #75738, #39968, #65614, #9623 ) ) ;
#18425=B_SPLINE_CURVE_WITH_KNOTS ( 'NONE', 3,
 ( #963, #100394, #8580, #1474 ),
 .UNSPECIFIED., .F., .F.,
 ( 4, 4 ),
 ( 0.000000000000000000, 9.999999999999592548E-05 ),
 .UNSPECIFIED. ) ;
#18426=DIRECTION ( 'NONE',  ( 3.773278334444166432E-23, -1.000000000000000000, 0.000000000000000000 ) ) ;
#18427=CARTESIAN_POINT ( 'NONE',  ( 18.33865528945960577, 14.04639130150205872, -1.500000000000002220 ) ) ;
#18430=CARTESIAN_POINT ( 'NONE',  ( -93.58414072440028519, -24.65952944569305316, 1.056160979905701458 ) ) ;
#18431=PLANE ( 'NONE',  #91165 ) ;
#18432=LINE ( 'NONE', #33151, #84735 ) ;
#18433=CARTESIAN_POINT ( 'NONE',  ( -105.6228709571500559, -23.85229601348997974, 10.88205029486207565 ) ) ;
#18434=CARTESIAN_POINT ( 'NONE',  ( -80.91017088437544658, -25.27183487616304447, 3.712349674769177987 ) ) ;
#18435=CARTESIAN_POINT ( 'NONE',  ( -69.41551097411255000, -25.24515161617911119, 5.862899549986941850 ) ) ;
#18436=CARTESIAN_POINT ( 'NONE',  ( -50.62287095715007013, -23.84047902841600930, -0.8780736468305810893 ) ) ;
#18437=CARTESIAN_POINT ( 'NONE',  ( -10.29545327866581950, 17.06371652956568852, 11.49999999999998934 ) ) ;
#18438=CARTESIAN_POINT ( 'NONE',  ( -75.56672023527714543, -23.48786465467241058, 11.44779295918254824 ) ) ;
#18439=CARTESIAN_POINT ( 'NONE',  ( 17.36586316225375981, 9.700842922841564686, -1.500000000000002220 ) ) ;
#18440=ORIENTED_EDGE ( 'NONE', *, *, #1862, .T. ) ;
#18441=CARTESIAN_POINT ( 'NONE',  ( -122.5228709571500758, -24.33927499327855770, 9.819080762295801179 ) ) ;
#18443=VECTOR ( 'NONE', #8043, 1000.000000000000114 ) ;
#18446=CARTESIAN_POINT ( 'NONE',  ( -80.58144581644191362, -24.92592662359561473, 8.075495903017996469 ) ) ;
#18447=CARTESIAN_POINT ( 'NONE',  ( 14.74948264216024008, 14.65492983226340407, 11.49999999999999645 ) ) ;
#18450=CARTESIAN_POINT ( 'NONE',  ( -50.61312830650895478, -25.18704472134033168, 3.308904489557473294 ) ) ;
#18451=CARTESIAN_POINT ( 'NONE',  ( 16.42120958226126604, -15.83219868413775622, 11.49999999999999645 ) ) ;
#18453=FACE_OUTER_BOUND ( 'NONE', #40672, .T. ) ;
#18454=CARTESIAN_POINT ( 'NONE',  ( -92.52287095715006160, -23.47596703998600631, 11.44779298504228393 ) ) ;
#18456=CARTESIAN_POINT ( 'NONE',  ( 18.20877288740043198, -8.745817889818592761, -1.500000000000002220 ) ) ;
#18457=CARTESIAN_POINT ( 'NONE',  ( -55.52287095715005449, -25.00158670708909270, 2.256160236439166411 ) ) ;
#18458=PLANE ( 'NONE',  #4802 ) ;
#18460=VERTEX_POINT ( 'NONE', #70255 ) ;
#18461=CARTESIAN_POINT ( 'NONE',  ( -109.5895376238167103, -24.64965694238407679, 8.947790433994649462 ) ) ;
#18462=CARTESIAN_POINT ( 'NONE',  ( -51.29687923781917647, -25.18439801854641047, 3.993462348633455061 ) ) ;
#18463=CARTESIAN_POINT ( 'NONE',  ( 2.999408428739025023, -19.78128511538675127, -1.500000000000002220 ) ) ;
#18464=CARTESIAN_POINT ( 'NONE',  ( 20.88312143257166653, -1.666129412636018214, 11.49999999999999645 ) ) ;
#18465=CARTESIAN_POINT ( 'NONE',  ( -29.35807781927573501, -25.00935022314251199, 7.267259836917594029 ) ) ;
#18467=CARTESIAN_POINT ( 'NONE',  ( 9.306852550357104903, -20.00191182576189064, 11.49999999999998934 ) ) ;
#18468=ADVANCED_FACE ( 'NONE', ( #24070 ), #64171, .F. ) ;
#18470=CARTESIAN_POINT ( 'NONE',  ( -40.20932372006943467, -25.27806103562203077, 5.067940379994220201 ) ) ;
#18472=DIRECTION ( 'NONE',  ( -3.773278334453079030E-23, 0.9999999999976377785, 2.173523156925979128E-06 ) ) ;
#18473=CARTESIAN_POINT ( 'NONE',  ( -118.6228709571500559, -24.64898659630368627, 1.056161002820833028 ) ) ;
#18474=CARTESIAN_POINT ( 'NONE',  ( -89.62287095715004170, -29.50247984919015209, -1.443849546365051806 ) ) ;
#18477=ORIENTED_EDGE ( 'NONE', *, *, #97862, .T. ) ;
#18478=B_SPLINE_CURVE_WITH_KNOTS ( 'NONE', 3,
 ( #97566, #20426, #74232, #4727, #6707, #28547, #74717, #52899, #52396, #35677, #59516, #66652, #13814, #20931, #76212, #44293, #12817, #97069 ),
 .UNSPECIFIED., .F., .F.,
 ( 4, 2, 2, 2, 2, 2, 2, 2, 4 ),
 ( 0.004711333090593606242, 0.005300197173489861781, 0.005889061256386118187, 0.006477925339282373726, 0.007066789422178629265, 0.007655653505074885672, 0.008244517587971140343, 0.008833381670867397617, 0.009422245753763653156 ),
 .UNSPECIFIED. ) ;
#18482=CARTESIAN_POINT ( 'NONE',  ( -51.52287095715007581, -24.33832256527048798, 0.1851278514138590403 ) ) ;
#18483=CARTESIAN_POINT ( 'NONE',  ( -20.35906544237474236, -2.577633573104691322, -1.500000000000002220 ) ) ;
#18485=DIRECTION ( 'NONE',  ( -3.773278334453079618E-23, 0.9999999999976377785, 2.173523156925979975E-06 ) ) ;
#18486=EDGE_CURVE ( 'NONE', #70518, #80790, #30321, .T. ) ;
#18489=CARTESIAN_POINT ( 'NONE',  ( 19.83320176327591255, -10.20924650237717835, -1.500000000000002220 ) ) ;
#18491=CARTESIAN_POINT ( 'NONE',  ( -124.6228709571500417, -24.51283580621365488, 0.6167428607019822540 ) ) ;
#18492=ORIENTED_EDGE ( 'NONE', *, *, #78006, .T. ) ;
#18493=CARTESIAN_POINT ( 'NONE',  ( -43.62287095715004881, -24.65952944569304606, 1.056160979905692576 ) ) ;
#18495=CARTESIAN_POINT ( 'NONE',  ( 7.204507412156021751, -19.57454612608841771, 11.49999999999998934 ) ) ;
#18499=ORIENTED_EDGE ( 'NONE', *, *, #80729, .T. ) ;
#18500=FACE_OUTER_BOUND ( 'NONE', #87251, .T. ) ;
#18501=CARTESIAN_POINT ( 'NONE',  ( -21.07084664159375009, 0.3847054351051909515, -1.500000000000002220 ) ) ;
#18502=ORIENTED_EDGE ( 'NONE', *, *, #41309, .F. ) ;
#18505=DIRECTION ( 'NONE',  ( 0.000000000000000000, -2.173523156925980399E-06, 0.9999999999976378895 ) ) ;
#18506=CARTESIAN_POINT ( 'NONE',  ( -86.50455038639833560, -24.51419770103155926, 9.386484678747184063 ) ) ;
#18507=CARTESIAN_POINT ( 'NONE',  ( -59.59827915153204714, -23.96119346886879597, -0.6495511937832131322 ) ) ;
#18508=CARTESIAN_POINT ( 'NONE',  ( -6.179238894844691465, -20.81818906610659425, -1.500000000000002220 ) ) ;
#18510=EDGE_CURVE ( 'NONE', #9237, #31838, #43638, .T. ) ;
#18511=CARTESIAN_POINT ( 'NONE',  ( -8.951960448472247478, 20.35530821588910300, 11.49999999999999645 ) ) ;
#18513=CARTESIAN_POINT ( 'NONE',  ( -50.49683564601712504, -25.31441722724132504, 5.199897239935473259 ) ) ;
#18515=CARTESIAN_POINT ( 'NONE',  ( -87.52287095715004739, -24.51283580621451108, 0.6167428607045201128 ) ) ;
#18516=VERTEX_POINT ( 'NONE', #56046 ) ;
#18521=VERTEX_POINT ( 'NONE', #63156 ) ;
#18524=CARTESIAN_POINT ( 'NONE',  ( -35.52287095715008292, -24.82558206586143257, 1.605769216559448820 ) ) ;
#18525=CARTESIAN_POINT ( 'NONE',  ( -105.5228709571501469, -24.63287334234180648, 0.9662140553045298619 ) ) ;
#18527=CARTESIAN_POINT ( 'NONE',  ( -130.5728709571500872, -25.35233180439156797, 6.153150975227889674 ) ) ;
#18528=CARTESIAN_POINT ( 'NONE',  ( -21.65924713590726469, 5.634197536097032888, -1.500000000000002220 ) ) ;
#18529=EDGE_CURVE ( 'NONE', #19170, #10252, #65410, .T. ) ;
#18531=CARTESIAN_POINT ( 'NONE',  ( -87.52287095715006160, -29.50248528299804818, 1.056150453629040253 ) ) ;
#18532=DIRECTION ( 'NONE',  ( 0.000000000000000000, -2.173523156925980399E-06, 0.9999999999976378895 ) ) ;
#18533=CARTESIAN_POINT ( 'NONE',  ( -44.62287095715004881, -23.48786465467240347, 11.44779295918255180 ) ) ;
#18534=DIRECTION ( 'NONE',  ( -3.773278334453079030E-23, 0.9999999999976377785, 2.173523156925979128E-06 ) ) ;
#18536=B_SPLINE_CURVE_WITH_KNOTS ( 'NONE', 3,
 ( #47816, #10248, #78738, #9239, #33589, #40201 ),
 .UNSPECIFIED., .F., .F.,
 ( 4, 2, 4 ),
 ( 1.570887131794952276E-05, 0.001396322306279762157, 0.002776935741241574537 ),
 .UNSPECIFIED. ) ;
#18537=B_SPLINE_CURVE_WITH_KNOTS ( 'NONE', 3,
 ( #14438, #98177, #99659, #45410 ),
 .UNSPECIFIED., .F., .F.,
 ( 4, 4 ),
 ( 0.000000000000000000, 1.000000000000000000 ),
 .UNSPECIFIED. ) ;
#18538=CARTESIAN_POINT ( 'NONE',  ( -63.93036092109726098, -24.37907397113049868, 9.703205396196695531 ) ) ;
#18539=CARTESIAN_POINT ( 'NONE',  ( 17.63768857353127828, -8.544740250177758512, -1.500000000000002220 ) ) ;
#18540=CARTESIAN_POINT ( 'NONE',  ( -50.28106314917847897, -25.31259380064802400, 4.732491477755599085 ) ) ;
#18541=VERTEX_POINT ( 'NONE', #48427 ) ;
#18543=CARTESIAN_POINT ( 'NONE',  ( -21.28347836979250118, 3.227085873532868021, -1.500000000000002220 ) ) ;
#18545=CARTESIAN_POINT ( 'NONE',  ( -81.42380231474228935, -25.30394809369661857, 5.197789011868366060 ) ) ;
#18546=CARTESIAN_POINT ( 'NONE',  ( -113.5228709571501327, -24.66019654487200441, 8.947790411086112172 ) ) ;
#18548=CARTESIAN_POINT ( 'NONE',  ( -12.73177969873712279, -19.06072230859735939, -1.500000000000002220 ) ) ;
#18550=CARTESIAN_POINT ( 'NONE',  ( -31.52287095715006160, -24.66019654487198665, 8.947790411086131712 ) ) ;
#18551=DIRECTION ( 'NONE',  ( -3.773278334444166432E-23, 1.000000000000000000, 0.000000000000000000 ) ) ;
#18552=CARTESIAN_POINT ( 'NONE',  ( 11.77038589110637901, 16.27938679534767275, 11.49999999999999645 ) ) ;
#18553=CARTESIAN_POINT ( 'NONE',  ( -110.3139465455115129, -25.10927396271619116, 2.832404819606896496 ) ) ;
#18555=CARTESIAN_POINT ( 'NONE',  ( -121.6228709571500417, -23.72773821059535848, 11.05748984161097503 ) ) ;
#18558=CARTESIAN_POINT ( 'NONE',  ( -17.59554656748941071, 9.132484154288260214, 11.49999999999998934 ) ) ;
#18560=CARTESIAN_POINT ( 'NONE',  ( 18.75866648459458830, -6.009157199652424453, -1.500000000000002220 ) ) ;
#18563=CARTESIAN_POINT ( 'NONE',  ( -57.52287095715005449, -24.50321055353803956, 9.387540953477520489 ) ) ;
#18565=CARTESIAN_POINT ( 'NONE',  ( -13.12974562303265813, -15.89414520977026513, 11.49999999999999645 ) ) ;
#18566=AXIS2_PLACEMENT_3D ( 'NONE', #38046, #54293, #29931 ) ;
#18568=CARTESIAN_POINT ( 'NONE',  ( 4.697487806458584991, -22.17256498326293013, 11.49999999999999645 ) ) ;
#18571=DIRECTION ( 'NONE',  ( -1.000000000000000000, -3.773278334444166432E-23, -8.201307841325785021E-29 ) ) ;
#18572=CARTESIAN_POINT ( 'NONE',  ( -97.51358978418939216, -24.15543982623907837, -0.2315651400026600415 ) ) ;
#18573=B_SPLINE_CURVE_WITH_KNOTS ( 'NONE', 3,
 ( #55632, #56636, #87062, #50021 ),
 .UNSPECIFIED., .F., .F.,
 ( 4, 4 ),
 ( 0.000000000000000000, 1.000000000000000000 ),
 .UNSPECIFIED. ) ;
#18574=CARTESIAN_POINT ( 'NONE',  ( -110.6228709571500417, -24.14406661707770141, 10.28769366152062226 ) ) ;
#18575=CARTESIAN_POINT ( 'NONE',  ( -93.52287095715006160, -24.64965694238407323, 8.947790433994196491 ) ) ;
#18577=CARTESIAN_POINT ( 'NONE',  ( 3.535601659403828201, -22.84449096179584160, 11.49999999999999645 ) ) ;
#18578=CARTESIAN_POINT ( 'NONE',  ( -21.78311099772515647, -6.823855485095160489, 11.49999999999998934 ) ) ;
#18579=PLANE ( 'NONE',  #82720 ) ;
#18580=CARTESIAN_POINT ( 'NONE',  ( -63.62365448271125956, -24.66019654487200086, 8.947790411086121054 ) ) ;
#18581=CARTESIAN_POINT ( 'NONE',  ( 8.356338879324495039, -20.90460381316865934, 11.49999999999999645 ) ) ;
#18582=ORIENTED_EDGE ( 'NONE', *, *, #91461, .T. ) ;
#18584=CARTESIAN_POINT ( 'NONE',  ( -19.92591009635028243, 9.278653061003369729, 11.49999999999998934 ) ) ;
#18585=CARTESIAN_POINT ( 'NONE',  ( -118.5228709571500758, -23.47596703998600631, 11.44779298504227860 ) ) ;
#18586=ADVANCED_FACE ( 'NONE', ( #76182 ), #30013, .F. ) ;
#18587=CARTESIAN_POINT ( 'NONE',  ( -111.5187080011053240, -23.96119346886881019, -0.6495511937832035843 ) ) ;
#18588=DIRECTION ( 'NONE',  ( -3.773278334453079618E-23, 0.9999999999976377785, 2.173523156925979975E-06 ) ) ;
#18589=ORIENTED_EDGE ( 'NONE', *, *, #12075, .F. ) ;
#18590=CARTESIAN_POINT ( 'NONE',  ( -48.50069532262279637, -24.15620529776628089, 10.23563542870660470 ) ) ;
#18591=CARTESIAN_POINT ( 'NONE',  ( -52.52287095715006870, -29.50248528299804818, 1.056150453629033370 ) ) ;
#18592=ORIENTED_EDGE ( 'NONE', *, *, #14290, .F. ) ;
#18593=EDGE_CURVE ( 'NONE', #45083, #21005, #38765, .T. ) ;
#18594=CARTESIAN_POINT ( 'NONE',  ( -54.58254524432665278, -24.51419770103157347, 9.386484678747176957 ) ) ;
#18595=CARTESIAN_POINT ( 'NONE',  ( 15.48611046165106941, -13.43736321338083783, 11.49999999999998934 ) ) ;
#18596=ORIENTED_EDGE ( 'NONE', *, *, #73131, .T. ) ;
#18597=EDGE_LOOP ( 'NONE', ( #54419, #46195, #78345, #38722 ) ) ;
#18599=CARTESIAN_POINT ( 'NONE',  ( -49.85569807066763559, -25.31193038000811057, 5.303933706555637784 ) ) ;
#18600=CARTESIAN_POINT ( 'NONE',  ( 22.67273400128462058, 4.441195646929153362, 11.49999999999998934 ) ) ;
#18601=CARTESIAN_POINT ( 'NONE',  ( -104.5531557358278008, -24.15620529776629155, 10.23563542870659759 ) ) ;
#18602=CARTESIAN_POINT ( 'NONE',  ( 19.78452974690265975, -4.759501717958375622, -1.500000000000002220 ) ) ;
#18603=ORIENTED_EDGE ( 'NONE', *, *, #8212, .F. ) ;
#18605=EDGE_CURVE ( 'NONE', #45470, #68982, #56942, .T. ) ;
#18606=CARTESIAN_POINT ( 'NONE',  ( -51.40142156539464935, -25.18959696641875112, 3.254916540799400515 ) ) ;
#18608=CARTESIAN_POINT ( 'NONE',  ( -105.5461413990837940, -25.00158670708910691, 2.256160236439218369 ) ) ;
#18609=CARTESIAN_POINT ( 'NONE',  ( -70.34543693012690824, -25.25855381946792377, 7.563173725924075441 ) ) ;
#18610=VERTEX_POINT ( 'NONE', #37134 ) ;
#18611=CARTESIAN_POINT ( 'NONE',  ( -28.88251580808842789, -25.21531814767515556, 2.994893284986237081 ) ) ;
#18612=CARTESIAN_POINT ( 'NONE',  ( -49.46456330771200527, -25.31573792550670277, 4.758318069380484516 ) ) ;
#18614=VECTOR ( 'NONE', #45404, 1000.000000000000114 ) ;
#18616=CARTESIAN_POINT ( 'NONE',  ( -8.830788454959730416, 18.81286502489961876, -1.500000000000002220 ) ) ;
#18617=ORIENTED_EDGE ( 'NONE', *, *, #45900, .F. ) ;
#18618=CARTESIAN_POINT ( 'NONE',  ( -125.6238070234729491, -24.83618233451450763, 1.606449574219537046 ) ) ;
#18620=CARTESIAN_POINT ( 'NONE',  ( -82.55620429048337883, -24.64898659630528854, 1.056161002820828143 ) ) ;
#18621=CARTESIAN_POINT ( 'NONE',  ( -102.6228709571500559, -24.64898659630368272, 1.056161002820829697 ) ) ;
#18623=ORIENTED_EDGE ( 'NONE', *, *, #73694, .T. ) ;
#18626=CARTESIAN_POINT ( 'NONE',  ( -43.57657991008606757, -24.66019654487199375, 8.947790411086121054 ) ) ;
#18627=EDGE_CURVE ( 'NONE', #85108, #85219, #85303, .T. ) ;
#18628=CARTESIAN_POINT ( 'NONE',  ( 10.81757466760856801, -19.22619917341675588, 11.49999999999999645 ) ) ;
#18630=CARTESIAN_POINT ( 'NONE',  ( -48.87380231474225667, -25.26256937810135028, 6.137091986423513390 ) ) ;
#18631=CARTESIAN_POINT ( 'NONE',  ( -18.09186581907994196, -13.49991075323410250, 11.49999999999998934 ) ) ;
#18632=PLANE ( 'NONE',  #99237 ) ;
#18637=EDGE_CURVE ( 'NONE', #96235, #7232, #32655, .T. ) ;
#18638=EDGE_CURVE ( 'NONE', #79877, #2526, #16833, .T. ) ;
#18640=ORIENTED_EDGE ( 'NONE', *, *, #38482, .F. ) ;
#18641=CARTESIAN_POINT ( 'NONE',  ( -20.81765089029956783, 3.879123387127271005, -1.500000000000002220 ) ) ;
#18642=CARTESIAN_POINT ( 'NONE',  ( -78.94558681842012504, -25.27791652114184373, 6.087055360511715030 ) ) ;
#18645=CARTESIAN_POINT ( 'NONE',  ( -22.15176777451872425, 1.842445310382735624, -1.500000000000002220 ) ) ;
#18646=CARTESIAN_POINT ( 'NONE',  ( -114.6244202119018922, -24.51314013834316086, 0.6176544820404237246 ) ) ;
#18648=VECTOR ( 'NONE', #34715, 1000.000000000000114 ) ;
#18651=CARTESIAN_POINT ( 'NONE',  ( -104.6228709571500559, -23.47593901973091235, -1.443836447539001089 ) ) ;
#18652=VECTOR ( 'NONE', #35707, 1000.000000000000114 ) ;
#18653=EDGE_CURVE ( 'NONE', #71190, #57577, #64140, .T. ) ;
#18654=CARTESIAN_POINT ( 'NONE',  ( -36.63501922174244640, -24.35071581493542325, 9.817618358456030592 ) ) ;
#18655=CARTESIAN_POINT ( 'NONE',  ( -40.45829750704998418, -25.18492896333868103, 3.293943116708551777 ) ) ;
#18656=EDGE_CURVE ( 'NONE', #41839, #40469, #15286, .T. ) ;
#18657=CARTESIAN_POINT ( 'NONE',  ( -7.007757480239389380, 18.17491015770016816, 11.49999999999998934 ) ) ;
#18658=CARTESIAN_POINT ( 'NONE',  ( -4.378498130703003532, 20.98420022172975763, 11.49999999999998934 ) ) ;
#18662=CARTESIAN_POINT ( 'NONE',  ( 7.803535043518188274, -21.38454823780343617, -1.500000000000002220 ) ) ;
#18664=EDGE_CURVE ( 'NONE', #61038, #32532, #570, .T. ) ;
#18666=CARTESIAN_POINT ( 'NONE',  ( -102.5982546441761940, -23.48783264082478439, -1.443836473390064601 ) ) ;
#18667=DIRECTION ( 'NONE',  ( -3.773278334453079030E-23, 0.9999999999976377785, 2.173523156925979128E-06 ) ) ;
#18668=CARTESIAN_POINT ( 'NONE',  ( -4.359361796094493258, -19.42695174060331809, 11.49999999999999645 ) ) ;
#18669=CARTESIAN_POINT ( 'NONE',  ( -104.5173987185542899, -23.96119346886880663, -0.6495511937832033622 ) ) ;
#18670=CARTESIAN_POINT ( 'NONE',  ( -48.62287095715004881, -29.50250243563736774, 8.947779886222146928 ) ) ;
#18671=CARTESIAN_POINT ( 'NONE',  ( -48.63355419739910701, -24.34968618360933590, 0.1864209137778884418 ) ) ;
#18672=ORIENTED_EDGE ( 'NONE', *, *, #99154, .F. ) ;
#18674=CARTESIAN_POINT ( 'NONE',  ( -31.81565132553424746, -25.16370864782812689, 7.203858152271859439 ) ) ;
#18675=CARTESIAN_POINT ( 'NONE',  ( 19.26462925850498920, -9.998780574493274287, 11.49999999999998934 ) ) ;
#18676=DIRECTION ( 'NONE',  ( -0.000000000000000000, 2.173523156925979552E-06, -0.9999999999976378895 ) ) ;
#18677=CARTESIAN_POINT ( 'NONE',  ( 14.28107258077893604, -13.35224110012613963, -1.500000000000002220 ) ) ;
#18682=CARTESIAN_POINT ( 'NONE',  ( -8.751980504941329286, -18.49744413911281882, 11.49999999999999645 ) ) ;
#18683=CARTESIAN_POINT ( 'NONE',  ( -49.62287095715004170, -23.47596703998600631, 11.44779298504227505 ) ) ;
#18685=ORIENTED_EDGE ( 'NONE', *, *, #3861, .T. ) ;
#18686=CARTESIAN_POINT ( 'NONE',  ( -62.62287095715003460, -24.51283580621364067, 0.6167428607019811437 ) ) ;
#18689=B_SPLINE_CURVE_WITH_KNOTS ( 'NONE', 3,
 ( #27198, #42930, #57164, #3870 ),
 .UNSPECIFIED., .F., .F.,
 ( 4, 4 ),
 ( 2.775557561562891351E-17, 0.0001000000000000167286 ),
 .UNSPECIFIED. ) ;
#18690=CARTESIAN_POINT ( 'NONE',  ( -63.55620429048340725, -23.47596703998600276, 11.44779298504227505 ) ) ;
#18693=CARTESIAN_POINT ( 'NONE',  ( -22.88579126497628025, -1.409509213828211927, 11.49999999999999645 ) ) ;
#18694=CARTESIAN_POINT ( 'NONE',  ( 21.15473741701296362, -8.388382055385795510, 11.49999999999998934 ) ) ;
#18697=CARTESIAN_POINT ( 'NONE',  ( -90.62932173586635543, -24.63355581998384380, 0.9682620441943978751 ) ) ;
#18699=CARTESIAN_POINT ( 'NONE',  ( -70.19980647797044071, -25.13395880908142388, 7.096976381558549818 ) ) ;
#18701=CARTESIAN_POINT ( 'NONE',  ( -12.54888962926113827, 17.92887824059606672, 11.49999999999998934 ) ) ;
#18702=CARTESIAN_POINT ( 'NONE',  ( -70.58953762381672448, -24.99132157543083821, 2.256160258750496084 ) ) ;
#18705=CARTESIAN_POINT ( 'NONE',  ( -26.31489179039940041, -24.86888853887588979, 3.386445682341310270 ) ) ;
#18706=DIRECTION ( 'NONE',  ( -1.000000000000000000, -3.773278334444165844E-23, -8.201307836089272790E-29 ) ) ;
#18707=CARTESIAN_POINT ( 'NONE',  ( -58.58294017270318221, -24.51314013834315020, 0.6176544820404091807 ) ) ;
#18709=ADVANCED_FACE ( 'NONE', ( #10696 ), #92624, .T. ) ;
#18710=CARTESIAN_POINT ( 'NONE',  ( -19.37329759448073574, 6.469241145865432863, -1.500000000000002220 ) ) ;
#18712=AXIS2_PLACEMENT_3D ( 'NONE', #21011, #59103, #43867 ) ;
#18713=ORIENTED_EDGE ( 'NONE', *, *, #61732, .F. ) ;
#18715=CARTESIAN_POINT ( 'NONE',  ( 22.99805582222048272, -0.5679727363130141482, 11.49999999999998934 ) ) ;
#18719=VERTEX_POINT ( 'NONE', #1081 ) ;
#18720=CARTESIAN_POINT ( 'NONE',  ( -97.62287095715004170, -24.65952944569304606, 1.056160979905701236 ) ) ;
#18721=EDGE_CURVE ( 'NONE', #12730, #80701, #18306, .T. ) ;
#18723=AXIS2_PLACEMENT_3D ( 'NONE', #58923, #12725, #83246 ) ;
#18725=CARTESIAN_POINT ( 'NONE',  ( -98.62287095715012697, -24.35013146730204525, 9.818937971375108376 ) ) ;
#18726=CARTESIAN_POINT ( 'NONE',  ( -99.62727544345402464, -24.35071581493543391, 9.817618358456025263 ) ) ;
#18727=CARTESIAN_POINT ( 'NONE',  ( -9.778911232092227124, -18.99720643767551209, 11.49999999999999645 ) ) ;
#18729=EDGE_CURVE ( 'NONE', #51651, #65785, #26557, .T. ) ;
#18731=CARTESIAN_POINT ( 'NONE',  ( 19.02167141253037030, -11.55642654327076535, -1.500000000000002220 ) ) ;
#18732=CARTESIAN_POINT ( 'NONE',  ( 18.97174343470660318, 8.267356841975738391, -1.500000000000002220 ) ) ;
#18733=ORIENTED_EDGE ( 'NONE', *, *, #45364, .T. ) ;
#18736=VERTEX_POINT ( 'NONE', #71601 ) ;
#18737=CARTESIAN_POINT ( 'NONE',  ( -56.52287095715007581, -24.50216790748205398, 0.6166512839542495072 ) ) ;
#18738=VERTEX_POINT ( 'NONE', #33032 ) ;
#18740=CARTESIAN_POINT ( 'NONE',  ( 7.117523389609132778, 19.69228268689324324, -1.500000000000002220 ) ) ;
#18741=EDGE_CURVE ( 'NONE', #14881, #60701, #63502, .T. ) ;
#18742=CARTESIAN_POINT ( 'NONE',  ( -18.33957545910867282, 11.93505917737106259, 11.49999999999999645 ) ) ;
#18743=DIRECTION ( 'NONE',  ( 3.773278334444166432E-23, -1.000000000000000000, 0.000000000000000000 ) ) ;
#18744=CARTESIAN_POINT ( 'NONE',  ( 12.95044643391442030, 18.39415735498938176, -1.500000000000002220 ) ) ;
#18745=CARTESIAN_POINT ( 'NONE',  ( 17.09260067683297635, -12.12037977771017871, 11.49999999999998934 ) ) ;
#18746=CARTESIAN_POINT ( 'NONE',  ( -38.50505405450132201, -23.96119346886880663, -0.6495511937831989213 ) ) ;
#18748=CARTESIAN_POINT ( 'NONE',  ( -89.52287095715006160, -23.47593901973090169, -1.443836447538996426 ) ) ;
#18750=VERTEX_POINT ( 'NONE', #78677 ) ;
#18755=ORIENTED_EDGE ( 'NONE', *, *, #38478, .T. ) ;
#18757=CARTESIAN_POINT ( 'NONE',  ( 8.370372042246325250, 19.68514866842044242, -1.500000000000002220 ) ) ;
#18760=CARTESIAN_POINT ( 'NONE',  ( 5.994809752082427501, 20.21905721239408393, -1.500000000000002220 ) ) ;
#18761=CARTESIAN_POINT ( 'NONE',  ( -73.52287095715007581, -29.50247984919015209, -1.443849546365055359 ) ) ;
#18762=DIRECTION ( 'NONE',  ( 0.000000000000000000, -2.173523156925980399E-06, 0.9999999999976378895 ) ) ;
#18763=CARTESIAN_POINT ( 'NONE',  ( -50.65001634216351789, -24.15602025860895452, 10.28564288303536856 ) ) ;
#18764=DIRECTION ( 'NONE',  ( -3.773278334453079618E-23, 0.9999999999976377785, 2.173523156925979975E-06 ) ) ;
#18766=CARTESIAN_POINT ( 'NONE',  ( -21.99024891984110752, 1.279939690139831665, -1.500000000000002220 ) ) ;
#18768=CARTESIAN_POINT ( 'NONE',  ( -65.60612770986470821, -23.85049219812685806, 10.88485053497527311 ) ) ;
#18769=DIRECTION ( 'NONE',  ( -1.000000000000000000, -3.773278334444166432E-23, -8.201307841325785021E-29 ) ) ;
#18770=CARTESIAN_POINT ( 'NONE',  ( -41.47025245262053517, -25.31624658460401278, 5.160615443078977016 ) ) ;
#18771=EDGE_CURVE ( 'NONE', #14381, #85963, #2098, .T. ) ;
#18772=CARTESIAN_POINT ( 'NONE',  ( -28.39339090630327789, -25.14676924958207849, 4.936952632524851836 ) ) ;
#18775=CARTESIAN_POINT ( 'NONE',  ( 20.90283063341239966, -4.354886778353011856, -1.500000000000002220 ) ) ;
#18776=CARTESIAN_POINT ( 'NONE',  ( -81.52287095715006160, -24.64898659630367916, 1.056161002820826145 ) ) ;
#18777=CARTESIAN_POINT ( 'NONE',  ( -48.85340342284951021, -25.32724633150700200, 4.398074151685130495 ) ) ;
#18778=EDGE_CURVE ( 'NONE', #27354, #95501, #9183, .T. ) ;
#18779=CARTESIAN_POINT ( 'NONE',  ( -64.59767640655398679, -23.96169478059713498, 10.65365249895718058 ) ) ;
#18780=CARTESIAN_POINT ( 'NONE',  ( -126.5228709571500616, -23.48786465467241769, 11.44779295918253581 ) ) ;
#18781=CARTESIAN_POINT ( 'NONE',  ( -8.190886813464794969, 21.05079722441571732, -1.500000000000002220 ) ) ;
#18782=VECTOR ( 'NONE', #40561, 1000.000000000000114 ) ;
#18783=CARTESIAN_POINT ( 'NONE',  ( -41.62287095715006302, -29.50250243563736774, 8.947779886222148704 ) ) ;
#18784=ORIENTED_EDGE ( 'NONE', *, *, #72044, .T. ) ;
#18786=CARTESIAN_POINT ( 'NONE',  ( -89.52287095715006160, -29.50248528299804818, 1.056150453629040253 ) ) ;
#18787=CARTESIAN_POINT ( 'NONE',  ( -79.55043832272009752, -24.15543982623907127, -0.2315651400026654261 ) ) ;
#18788=CARTESIAN_POINT ( 'NONE',  ( -16.88869819569221065, 10.18974688345344148, 11.49999999999999645 ) ) ;
#18789=CARTESIAN_POINT ( 'NONE',  ( -55.58953762381671737, -25.00182538069145011, 7.747789668545099317 ) ) ;
#18791=CARTESIAN_POINT ( 'NONE',  ( -96.55620429048340725, -23.47593901973091235, -1.443836447539001089 ) ) ;
#18792=EDGE_CURVE ( 'NONE', #48449, #98958, #3559, .T. ) ;
#18793=ORIENTED_EDGE ( 'NONE', *, *, #75754, .F. ) ;
#18796=CARTESIAN_POINT ( 'NONE',  ( -70.52287095715007581, -24.92604778743017491, 8.074972756849348343 ) ) ;
#18797=CARTESIAN_POINT ( 'NONE',  ( -124.5557933546448908, -23.96169478059714564, 10.65365249895717170 ) ) ;
#18798=CARTESIAN_POINT ( 'NONE',  ( 0.9236959384754221958, 21.56878955078795812, 11.49999999999998934 ) ) ;
#18799=DIRECTION ( 'NONE',  ( 3.773278334444166432E-23, -1.000000000000000000, 0.000000000000000000 ) ) ;
#18801=CARTESIAN_POINT ( 'NONE',  ( -95.52287095715010423, -24.92604778743017846, 8.074972756849360778 ) ) ;
#18802=CARTESIAN_POINT ( 'NONE',  ( -28.52287095715005805, -23.31185441368106126, 11.44779303854528685 ) ) ;
#18804=CARTESIAN_POINT ( 'NONE',  ( -19.19514693104756375, 4.742496307885142315, 11.49999999999998934 ) ) ;
#18805=ORIENTED_EDGE ( 'NONE', *, *, #88074, .F. ) ;
#18806=CARTESIAN_POINT ( 'NONE',  ( 18.81862293822770837, 7.596102252255398035, 11.49999999999999645 ) ) ;
#18808=ORIENTED_EDGE ( 'NONE', *, *, #46692, .T. ) ;
#18809=CARTESIAN_POINT ( 'NONE',  ( -110.6228709571500133, -24.15431212366391733, -0.2830839119429083839 ) ) ;
#18810=PLANE ( 'NONE',  #78279 ) ;
#18814=CARTESIAN_POINT ( 'NONE',  ( -71.62287095715004170, -23.72747288104470087, -1.053458166803226570 ) ) ;
#18815=CARTESIAN_POINT ( 'NONE',  ( 4.692034869050136336, 19.47840706813412126, 11.49999999999998934 ) ) ;
#18817=ORIENTED_EDGE ( 'NONE', *, *, #70085, .T. ) ;
#18819=B_SPLINE_CURVE_WITH_KNOTS ( 'NONE', 3,
 ( #45958, #54076, #30212, #76381, #13490, #14989 ),
 .UNSPECIFIED., .F., .F.,
 ( 4, 2, 4 ),
 ( 1.570887131795109485E-05, 0.001396322306279764976, 0.002776935741241578874 ),
 .UNSPECIFIED. ) ;
#18823=CARTESIAN_POINT ( 'NONE',  ( -113.5228709571500474, -24.50216790748205398, 0.6166512839542556135 ) ) ;
#18827=DIRECTION ( 'NONE',  ( 3.773278334444166432E-23, -1.000000000000000000, 0.000000000000000000 ) ) ;
#18828=ORIENTED_EDGE ( 'NONE', *, *, #18638, .T. ) ;
#18829=EDGE_CURVE ( 'NONE', #89496, #25882, #41123, .T. ) ;
#18830=CARTESIAN_POINT ( 'NONE',  ( -3.780122020211411193, 19.97858748211865532, -1.500000000000002220 ) ) ;
#18832=ADVANCED_FACE ( 'NONE', ( #28400 ), #35538, .T. ) ;
#18833=CARTESIAN_POINT ( 'NONE',  ( -21.95939045666098366, -6.591442671832903777, -1.500000000000002220 ) ) ;
#18834=CARTESIAN_POINT ( 'NONE',  ( -32.61005697994687580, -23.73766607897670866, -1.055555164236442023 ) ) ;
#18835=EDGE_CURVE ( 'NONE', #33008, #12032, #19355, .T. ) ;
#18836=CARTESIAN_POINT ( 'NONE',  ( -122.5228709571500900, -24.34917612406837861, 0.1852690917426592365 ) ) ;
#18837=EDGE_LOOP ( 'NONE', ( #84392, #78361, #12890, #86324 ) ) ;
#18838=FACE_OUTER_BOUND ( 'NONE', #83190, .T. ) ;
#18839=EDGE_CURVE ( 'NONE', #93507, #4166, #37517, .T. ) ;
#18842=CARTESIAN_POINT ( 'NONE',  ( -65.62287095715005592, -24.14406661707770496, 10.28769366152061160 ) ) ;
#18843=CARTESIAN_POINT ( 'NONE',  ( -16.84575021678815432, -12.90291372800108505, 11.49999999999999645 ) ) ;
#18844=CARTESIAN_POINT ( 'NONE',  ( -17.14978611337857473, 13.99085498846200437, -1.500000000000002220 ) ) ;
#18845=CARTESIAN_POINT ( 'NONE',  ( 17.26003113218828489, 11.23261964116016642, -1.500000000000002220 ) ) ;
#18846=AXIS2_PLACEMENT_3D ( 'NONE', #60493, #91410, #54372 ) ;
#18848=CARTESIAN_POINT ( 'NONE',  ( -111.5895376238167245, -23.48783264082479505, -1.443836473390060604 ) ) ;
#18852=ORIENTED_EDGE ( 'NONE', *, *, #23672, .F. ) ;
#18857=CARTESIAN_POINT ( 'NONE',  ( -83.62287095715007013, -24.65952944569304606, 1.056160979905700792 ) ) ;
#18858=B_SPLINE_CURVE_WITH_KNOTS ( 'NONE', 3,
 ( #48054, #9982, #10986, #49562, #40936, #63292, #72396, #71898, #2383, #80492, #72896, #34328, #78984, #55678, #9483, #1878, #95223, #63802 ),
 .UNSPECIFIED., .F., .F.,
 ( 4, 2, 2, 2, 2, 2, 2, 2, 4 ),
 ( 4.336808689942017736E-18, 0.0005889077912318099479, 0.001177815582463615559, 0.001766723373695421170, 0.002355631164927226781, 0.002944538956159032175, 0.003533446747390838003, 0.004122354538622643831, 0.004711262329854449225 ),
 .UNSPECIFIED. ) ;
#18859=CARTESIAN_POINT ( 'NONE',  ( -28.65224025812264586, -23.80901598000311026, 10.65365253163527015 ) ) ;
#18861=CARTESIAN_POINT ( 'NONE',  ( -15.27568272636907665, 14.01247568063241999, -1.500000000000002220 ) ) ;
#18862=CARTESIAN_POINT ( 'NONE',  ( -6.878457297428972161, 20.61903435171069532, 11.49999999999999645 ) ) ;
#18866=CARTESIAN_POINT ( 'NONE',  ( 18.93296920960566965, -11.98514031388154599, 11.49999999999998934 ) ) ;
#18871=CARTESIAN_POINT ( 'NONE',  ( -84.62287095715005592, -24.64898659630367561, 1.056161002820826145 ) ) ;
#18877=CARTESIAN_POINT ( 'NONE',  ( 10.86157628581156764, 18.25448884030880592, -1.500000000000002220 ) ) ;
#18879=CARTESIAN_POINT ( 'NONE',  ( -101.1944152955115044, -25.16311295231453826, 6.858246048749960799 ) ) ;
#18880=CARTESIAN_POINT ( 'NONE',  ( 12.52028139621776326, 17.89958603277719718, -1.500000000000002220 ) ) ;
#18881=CARTESIAN_POINT ( 'NONE',  ( -52.56018670930887993, -23.73791477778911840, 11.05961554403171476 ) ) ;
#18882=CARTESIAN_POINT ( 'NONE',  ( -41.35158263814751933, -25.18430974066979999, 3.766621014227882203 ) ) ;
#18883=CARTESIAN_POINT ( 'NONE',  ( -35.62287095715005592, -23.47593901973091235, -1.443836447539011525 ) ) ;
#18884=CARTESIAN_POINT ( 'NONE',  ( 21.83686239284238084, -0.8075297431944471471, -1.500000000000002220 ) ) ;
#18888=DIRECTION ( 'NONE',  ( -3.773278334453080206E-23, 0.9999999999976377785, 2.173523156925979975E-06 ) ) ;
#18891=CARTESIAN_POINT ( 'NONE',  ( -32.52287095715006160, -23.47596703998600631, 11.44779298504229459 ) ) ;
#18894=CARTESIAN_POINT ( 'NONE',  ( -10.24610470412292607, -22.99878645841938507, 0.8294870405985478312 ) ) ;
#18895=CARTESIAN_POINT ( 'NONE',  ( -13.59518820711925358, -16.35513075224449864, -1.500000000000002220 ) ) ;
#18899=DIRECTION ( 'NONE',  ( -3.773278334453079030E-23, 0.9999999999976377785, 2.173523156925979128E-06 ) ) ;
#18900=DIRECTION ( 'NONE',  ( 0.000000000000000000, 0.9999999999976377785, 2.173523156925979128E-06 ) ) ;
#18901=CARTESIAN_POINT ( 'NONE',  ( 7.440116899146960172, 17.95454168335740874, 11.49999999999998934 ) ) ;
#18902=ADVANCED_FACE ( 'NONE', ( #81202 ), #25564, .T. ) ;
#18905=CARTESIAN_POINT ( 'NONE',  ( -18.23851433863309879, 7.102826447048048664, 11.49999999999999645 ) ) ;
#18907=CARTESIAN_POINT ( 'NONE',  ( -42.62287095715004881, -23.48786465467240347, 11.44779295918255180 ) ) ;
#18908=ORIENTED_EDGE ( 'NONE', *, *, #35129, .F. ) ;
#18909=CARTESIAN_POINT ( 'NONE',  ( -39.56136241089613037, -25.29384247623274362, 5.536731341526268224 ) ) ;
#18910=CARTESIAN_POINT ( 'NONE',  ( -89.63826309510754697, -23.73766607897671221, -1.055555164236434029 ) ) ;
#18912=DIRECTION ( 'NONE',  ( -3.773278334453079618E-23, 0.9999999999976377785, 2.173523156925979975E-06 ) ) ;
#18913=B_SPLINE_CURVE_WITH_KNOTS ( 'NONE', 3,
 ( #25561, #56531, #77332, #718 ),
 .UNSPECIFIED., .F., .F.,
 ( 4, 4 ),
 ( 0.000000000000000000, 9.999999999998897304E-05 ),
 .UNSPECIFIED. ) ;
#18914=CARTESIAN_POINT ( 'NONE',  ( -81.23841534186585989, -25.24813948233231642, 7.364952454261663561 ) ) ;
#18915=CARTESIAN_POINT ( 'NONE',  ( 9.442166470422634461, 17.27452087139410963, 11.49999999999998934 ) ) ;
#18917=CARTESIAN_POINT ( 'NONE',  ( -33.52287095715006160, -29.50250786944525672, 11.44777988621624409 ) ) ;
#18918=DIRECTION ( 'NONE',  ( -3.773278334444167608E-23, 1.000000000000000000, 0.000000000000000000 ) ) ;
#18923=CARTESIAN_POINT ( 'NONE',  ( -72.52287095715007581, -23.47593901973090169, -1.443836447538996870 ) ) ;
#18924=CARTESIAN_POINT ( 'NONE',  ( -47.59972484022089390, -23.96119346886880663, -0.6495511937831951466 ) ) ;
#18925=CARTESIAN_POINT ( 'NONE',  ( -105.6228709571500133, -24.83620972994591725, 8.398175272781362111 ) ) ;
#18930=DIRECTION ( 'NONE',  ( -1.000000000000000000, -3.773278334444167608E-23, -8.201307833595939069E-29 ) ) ;
#18931=CARTESIAN_POINT ( 'NONE',  ( -2.986242917674419850, -19.73498743542299749, 11.49999999999998934 ) ) ;
#18932=FACE_OUTER_BOUND ( 'NONE', #81779, .T. ) ;
#18933=CARTESIAN_POINT ( 'NONE',  ( -14.63867168220055781, -13.42826565525684579, -1.500000000000002220 ) ) ;
#18934=VERTEX_POINT ( 'NONE', #69107 ) ;
#18938=FACE_OUTER_BOUND ( 'NONE', #40573, .T. ) ;
#18941=CARTESIAN_POINT ( 'NONE',  ( 10.19739565540945492, -18.13666118385682680, 11.49999999999999645 ) ) ;
#18944=CARTESIAN_POINT ( 'NONE',  ( 13.72848742581335912, -18.28091200367991576, 11.49999999999999645 ) ) ;
#18946=CARTESIAN_POINT ( 'NONE',  ( -116.6228709571500559, -29.50247984919015209, -1.443849546365046699 ) ) ;
#18947=B_SPLINE_CURVE_WITH_KNOTS ( 'NONE', 3,
 ( #33514, #47745, #70571, #18291, #1067, #41641 ),
 .UNSPECIFIED., .F., .F.,
 ( 4, 2, 4 ),
 ( 6.391158118972358895E-06, 0.001387004593080794169, 0.002767618028042615873 ),
 .UNSPECIFIED. ) ;
#18948=CARTESIAN_POINT ( 'NONE',  ( -89.62287095715004170, -23.47596703998600631, 11.44779298504227860 ) ) ;
#18949=VERTEX_POINT ( 'NONE', #36667 ) ;
#18950=EDGE_CURVE ( 'NONE', #28719, #53939, #66483, .T. ) ;
#18951=B_SPLINE_CURVE_WITH_KNOTS ( 'NONE', 3,
 ( #89010, #19986, #50952, #12367, #35723, #90003 ),
 .UNSPECIFIED., .F., .F.,
 ( 4, 2, 4 ),
 ( 1.570887131794333942E-05, 0.001396322306279758037, 0.002776935741241572803 ),
 .UNSPECIFIED. ) ;
#18952=CARTESIAN_POINT ( 'NONE',  ( -5.512817753899047268, 19.46650688538001361, 11.49999999999998934 ) ) ;
#18954=CARTESIAN_POINT ( 'NONE',  ( -123.6228709571500559, -23.47593901973091235, -1.443836447538997536 ) ) ;
#18955=EDGE_CURVE ( 'NONE', #46348, #25493, #5718, .T. ) ;
#18956=CARTESIAN_POINT ( 'NONE',  ( -111.6228709571500701, -23.48786465467241769, 11.44779295918254114 ) ) ;
#18957=EDGE_CURVE ( 'NONE', #97111, #15522, #83336, .T. ) ;
#18958=ORIENTED_EDGE ( 'NONE', *, *, #57500, .T. ) ;
#18959=CARTESIAN_POINT ( 'NONE',  ( -79.62531161443044425, -25.31170139299580413, 4.690176232765736586 ) ) ;
#18961=CARTESIAN_POINT ( 'NONE',  ( 17.55240489776628721, -9.587225365216566431, -1.500000000000002220 ) ) ;
#18963=CARTESIAN_POINT ( 'NONE',  ( 6.892386425805808514, -19.84609432511738447, 11.49999999999999645 ) ) ;
#18965=CARTESIAN_POINT ( 'NONE',  ( -29.81066036315064949, -25.25719168430799044, 5.128783157772433654 ) ) ;
#18967=CARTESIAN_POINT ( 'NONE',  ( 19.90762846840230083, -9.494064324355022677, -1.500000000000002220 ) ) ;
#18969=CARTESIAN_POINT ( 'NONE',  ( -39.54917078480641379, -25.31589227305247647, 4.610327192741620728 ) ) ;
#18970=CARTESIAN_POINT ( 'NONE',  ( -95.62287095715005592, -29.50247984919015209, -1.443849546365050029 ) ) ;
#18971=CARTESIAN_POINT ( 'NONE',  ( -72.54160130282839702, -24.51314013834316796, 0.6176544820404143987 ) ) ;
#18973=ORIENTED_EDGE ( 'NONE', *, *, #71438, .T. ) ;
#18976=CARTESIAN_POINT ( 'NONE',  ( -84.62287095715005592, -23.47593901973091235, -1.443836447539004642 ) ) ;
#18979=CARTESIAN_POINT ( 'NONE',  ( -1.317410511717131971, -20.46822056820986546, -1.500000000000002220 ) ) ;
#18983=CARTESIAN_POINT ( 'NONE',  ( -41.52287095715006870, -23.47596703998600631, 11.44779298504229281 ) ) ;
#18984=CARTESIAN_POINT ( 'NONE',  ( -19.39139147909919458, -11.06001032434818576, 11.49999999999998934 ) ) ;
#18989=CARTESIAN_POINT ( 'NONE',  ( -32.62287095715004881, -24.64965695001467694, 8.947790433994189385 ) ) ;
#18991=B_SPLINE_CURVE_WITH_KNOTS ( 'NONE', 3,
 ( #69451, #100369, #92774, #23259, #56747, #35268, #43382, #50994, #41506, #97159, #35765, #2954, #59604, #87678, #36260, #66233, #66735, #4812, #87174, #5801, #95290, #90535, #67224, #98137, #82421, #44377, #20516, #97648, #27653, #74320, #58598, #82915, #72459, #18161, #5301, #25774, #17661, #28150, #21017, #41008, #28644, #59108, #74805, #90046, #51986, #20028, #12408, #13403, #51487, #89545, #43872, #81929, #12905, #75303, #67722, #36757, #25269, #49133, #80060, #56248, #48632, #64368, #79559, #10048, #10545, #71965, #2446, #33379, #92525, #68207, #37748, #98636, #83415, #60110, #69706, #99626, #68708, #14400, #77292, #76296, #61103, #92031, #53496, #30128, #93021, #44880, #31127, #22503, #7795, #85414, #15398, #53987, #22004, #99135, #84421, #45381, #77788, #84914, #52485, #6791, #14899, #29635, #60609, #29136, #52989, #13902, #23498, #91034, #45868, #54477, #15900, #75801, #91531, #83922, #21508, #76785, #6301, #46865, #37259, #7288, #8297, #38239, #69197, #30631, #100114, #61608, #39241, #22999, #46360, #38738, #185, #62101, #40254, #48876, #49381, #16908, #80313, #64115, #78295, #8802, #1194, #48373, #93519, #54981, #24014, #71204, #25015, #25526, #56498, #87420, #94030, #55994, #94531, #71708, #18413, #72211, #95035, #33643, #10300, #79803, #17918, #26023, #41258, #86919, #87929, #39741, #683, #17412, #70199, #62594, #79302, #10803, #16398, #64623, #32129, #2701, #85926, #9799, #95536, #2206, #56993, #31629, #47367, #70699, #63102, #40750, #55484, #24516, #86422, #47871, #78791, #33135, #9289, #1700, #32632, #63610, #34646, #80817, #98013, #20894, #65615, #96533, #50871, #4193, #27027, #27532, #5182, #51365, #49885, #35643, #73212, #73699, #96038, #57996, #20390, #88931, #82304, #35146, #97036, #66117, #36136, #74687, #11794, #12783, #28514, #58985, #97528, #19403, #42282, #58489, #50374, #51867, #28027, #26532, #81312, #89426, #18905, #59477, #42766, #43752, #19898, #67105, #81810, #90418, #82798, #89921, #41769, #12284, #3700, #43260, #74202, #72712, #3209, #57497, #4693, #66616, #34151, #65118, #88431, #11300, #99509, #38625, #13281, #52860, #69588, #23382, #52362, #37627, #68, #92905, #30007, #83798, #60488, #91907, #84293, #15280, #22382, #44255, #61979, #54366, #99011, #7171, #21385, #83296, #44752, #21882, #60979, #68584, #29508, #14278, #53367, #91405, #46243, #75676, #22877, #45251, #14779, #45744, #75183, #5677, #13776, #77173, #53865, #84797, #69076, #31012, #38120, #76666, #76176, #100001, #6674, #36629, #30511, #6176, #92405, #37129, #67597, #61480, #7679, #29013, #98515, #59983, #90917, #68088, #10187, #78670, #71092, #17802, #79189, #86305, #2091, #24403, #86803, #17293, #25909, #9178, #64508, #85809, #47251, #95421, #40139, #23898, #41148, #85297, #8689, #15785, #72100, #1076, #9685, #54868, #55371, #46750, #70081, #77673, #56383, #16790, #47756, #32017, #64003, #62991, #33027, #39124, #93912, #1584, #32521, #94917, #25408, #63496, #94417, #39628, #2585, #8184, #70583, #71595, #78176, #62477, #48258, #24900, #55878, #565, #40644, #87303, #48764, #79690, #33522, #31514, #93404, #16289, #42158, #43635, #73589, #34027, #5065, #12171, #35029, #80198, #41650, #10689, #57881, #11672, #43142, #18788, #66503, #65501, #96921, #66001, #18301, #36013, #26414, #3091, #49271, #26910, #12673, #19285, #74575, #50754, #4077, #66988, #95920, #87813, #81196, #49767, #35532, #57387, #72596, #27414, #20276, #65004, #97417, #4583, #11186, #42655, #88315, #27906, #74090, #97901, #56883, #80697, #58373, #73096, #58862, #89311, #3586, #50256, #34529, #96423, #88819, #19780, #81699, #89806, #51246, #82186, #38513, #77060, #52250, #37514, #91301, #13661, #14164, #92296, #38014, #90303, #99888, #29398, #67981, #44633, #7064, #6061, #21770, #5563, #46135, #37017, #30395, #45141, #7564, #75561, #22767, #83683, #28903, #51751, #76068, #59869, #6567, #98903, #68471, #69464, #60377, #53754, #99405, #90805, #82684, #29899, #20773, #52744, #28395, #61368, #45635, #59358, #60867, #84682, #13165, #76555, #68964, #91790, #22268, #83177, #44136, #75063, #53252, #14671, #21274, #36509, #84181, #15168, #67474, #98399, #47640, #69962, #93287, #94795, #41026, #79067, #79574, #47139, #10065, #94292, #8063, #39009, #31402, #8569, #16670, #24291, #16171, #70469, #9063, #78055, #32909, #62361, #9560, #39517, #40014, #1463, #48650, #1967, #24778, #63881, #40528, #71479, #55758, #17675, #86685, #78556, #954, #70973, #31904, #56263, #62879, #23782, #25284, #447, #61866, #87188, #54755, #100386, #92790, #32406, #48141, #63379, #30899, #93796, #86188, #23271, #17172, #55257, #54254, #85184, #15673, #46640, #77558, #85690, #51126, #97301, #27785, #25788, #64887, #10561, #58738, #82070, #95797, #12556, #89687, #88197, #65879, #41522, #11066, #71979, #56763, #33394, #43021, #72978, #42032, #26291, #50627, #18668, #12052, #65382, #26790, #3468, #66371, #42533, #73965, #50134, #2461, #20164, #64386, #57267, #95303, #88697, #49151, #87693, #27293, #19165, #96302, #49642, #34405, #81078, #80572, #4463, #33902, #81581, #57754, #11554, #73467, #18177, #80077, #72476, #2969, #3961, #34905, #96799, #58248, #89193, #19662, #35414, #91174, #83050, #99764, #59746, #5443, #22147, #44007, #4951, #21648, #6940, #59240, #53134, #91668, #98277, #29279, #66864, #84061, #60250, #76435, #37401, #44513, #60746, #13543, #45021, #75941, #84559, #36894, #22643, #74939, #36395, #53635, #67858, #14546, #52621, #75438, #43521, #92171, #68846, #90679, #68349, #13046, #5938, #74457, #28281, #35896, #45519, #98779, #83557, #21159, #37894, #52127, #14040, #20658, #61248, #6445, #30270, #99282, #97789, #29779, #90183, #51629, #82564, #67357, #28783, #15544, #828, #31273, #94674, #70849, #69340, #93162, #31780, #23652, #32277, #63246, #85559, #62751, #40399, #15043, #54625, #71352, #25158, #54132, #39391, #1841, #56135, #93668, #16042, #62242, #24160, #47010, #77930, #94170, #8442, #70345, #92666, #32779, #55130, #9436, #61747, #48016, #86064, #24654, #63759, #55634, #1341, #38885, #46506, #16538, #47514, #46015, #86565, #100259, #78439, #8940, #39889, #17049, #76934, #69847, #30777, #7432, #38387, #78941, #23144, #85057, #77434, #7936, #327, #66257, #3356, #57141, #33783, #65265, #57634, #89072, #96188, #17555, #97181, #64768, #27675, #80958, #95182, #25666, #18054, #95683, #34291, #10948, #2850, #88078, #26676, #26167, #19548, #49021, #96675, #18552, #88576, #19050, #35292, #50508, #11442, #81465, #27175, #58136, #42421, #4342, #73352, #50023, #49524, #3846, #80456, #42906, #41913, #79952, #65757, #87569, #48521, #34786, #2344, #11940, #73842, #41400, #72855, #9941, #87064, #79449, #40893, #71855, #33273, #64260, #72354, #56638, #10438, #6323, #36286, #13427, #37773, #83944, #68728, #52008, #37279, #75327, #28665, #99647, #6815, #82446, #67744, #21039, #43896, #44400, #22026, #68230, #66756, #52508, #90066, #74341, #99159, #29657, #60632, #60133, #14424, #82938, #5822, #91553, #83437, #59627, #75824, #98160, #91057, #21531, #58624, #36780, #89569, #59130, #20539, #20053, #98661, #53014, #45399, #51015, #12927, #81951, #76316, #74829, #13926, #28171, #90559, #12435, #43405, #4833, #35786, #29159, #44902, #5323, #97674, #67243, #51512, #7309, #86818, #63508, #25922, #76810, #64523, #1595, #41160, #18316, #48781, #87317, #55381, #30658, #17306, #47769, #10705, #17815, #84440, #9190, #48270, #40150, #93923, #61124, #86320, #14920, #56898, #30150, #71106, #87830, #41670, #69220, #55891, #49285, #72610, #79201, #32534, #78683, #9699, #2106, #33538, #40659, #10202, #92053, #94428, #22523, #25423, #38262, #100135, #63004, #24914, #71608, #33039, #64020, #94934, #56397, #79704, #95435, #24416, #72113, #2604, #80212, #53517, #45893, #16803, #27921, #67005, #43652, #12688, #58882, #20792, #97436, #81713, #42671, #50772, #73604, #59376, #19304, #65519, #82205, #3600, #65021, #97917, #34545, #51767, #26929, #12185, #66019, #88835, #89328, #28410, #74589, #11201, #89821, #96437, #35046, #57402, #57898, #5081, #50271, #3109, #82701, #96937, #90320, #49784, #36032, #4095, #13180, #44150, #20291, #51265, #81214, #11688, #19797, #27431, #34044, #95935, #88330, #58391, #43163, #74105, #26436, #18806, #4599, #80717, #42174, #73113, #35547, #66517, #85198, #13681, #99419, #30913, #54272, #91810, #45157, #21784, #53266, #45649, #77074, #84194, #5580, #15689, #52761, #75084, #68977, #83193, #44648, #6079, #83698, #22283, #29913, #91315, #76080, #14684, #14180, #7579, #37031, #84696, #6579, #76574, #7079, #23287, #38527, #99902, #69485, #15187, #46150, #30414, #92805, #61382, #38028, #37534, #92310, #68484, #61883, #60879, #67993, #53769, #75577, #36525, #22780, #98919, #100400, #67493, #98415, #28918, #59887, #90819, #21293, #52264, #29412, #60392, #47656, #63901, #86206, #48156, #79081, #87709, #40032, #25807, #47155, #2479, #462, #39533, #85707, #33410, #56777, #70486, #16185, #64402, #46655, #969, #77574, #71996, #62893, #40543, #78072, #16685, #8079, #31418, #39026, #78571, #9077, #93814, #70991, #95319, #69978, #62375, #93303, #24304, #48667, #63392, #23796, #55270, #10081, #1482, #8584, #54770, #32420, #31923, #94309, #24796, #55774, #1982, #86699, #17187, #9581, #71493, #94812, #25299, #32923, #56279, #87202, #17693, #79589, #41040, #4480, #80590, #95812, #50645, #42051, #34921, #88711, #65402, #96814, #89209, #20179, #27306, #49166, #66882, #59258, #3482, #4965, #65895, #26311, #97806, #73983, #58269, #41541, #2986, #72492, #19676, #96319, #51142, #11081, #27801, #26808, #81594, #12066, #80092, #28299, #88215, #64903, #10576, #19183, #74474, #81092, #35913, #43040, #35428, #18195, #57769, #33923, #34422, #72994, #97317, #18682, #57284, #66390, #82090, #49657, #58755, #89708, #50153, #3979, #11569, #12573, #43537, #42548, #73480, #38405, #6959, #29295, #91684, #22166, #30798, #83575, #69360, #90700, #52142, #100277, #14059, #51648, #90199, #59765, #36412, #82587, #60268, #46034, #52639, #76955, #68366, #91191, #37420, #21664, #7449, #5955, #83067, #68861, #21178, #13063, #99302, #53651, #5461, #99779, #37911, #44531, #75957, #44022, #30287, #76454, #22663, #84076, #45039, #61266, #6463, #53151, #14566, #20678, #29796, #74959, #13562, #75455, #67375, #60762, #92187, #45534, #84575, #98293, #28799, #36910, #67873, #15066, #98802, #846, #61763, #46524, #23162, #32795, #62769, #31801, #77947, #24176, #17570, #54154, #92682, #79468, #39409, #63776, #78454, #40910, #93687, #71371, #48542, #78957, #17065, #85576, #62258, #47532, #8460, #71870, #48032, #15563, #70361, #8957, #55150, #9458, #40415, #86079, #39905, #16058, #85077, #16556, #87080, #2358, #343, #70870, #9959, #77453, #1360, #32295, #63266, #94184, #24670, #94690, #55651, #7953, #38907, #69863, #47031, #31291, #93185, #23670, #54644, #86579, #1854, #25176, #56151, #3372, #42433, #10963, #66270, #95698, #42924, #41929, #73368, #11459, #72870, #33289, #97193, #50522, #87590, #34304, #50039, #65283, #81480, #11953, #96205, #19064, #88097, #51027, #95198, #18565, #19565, #26186, #10453, #65776, #57159, #26691, #43422, #80972, #3864, #34803, #35308, #96690, #64276, #81972, #74354, #49540, #20065, #27191, #41416, #12450, #89087, #58149, #56653, #18070, #49040, #57650, #88591, #73860, #80470, #4359, #27692, #58638, #89585, #25682, #79967, #2867, #72372, #33799, #64782, #61142, #67757, #92067, #99173, #21547, #22537, #43910, #35799, #29172, #97690, #83453, #84454, #51527, #68742, #36300, #37790, #28185, #44916, #53028, #6337, #30166, #98679, #91071, #99660, #29674, #5840, #22046, #44417, #37297, #83959, #82950, #60150, #14937, #53529, #45909, #59142, #98178, #74841, #4845, #66772, #28680, #90083, #20558, #21053, #60644, #5344, #75340, #82462, #12941, #91565, #67256, #36795, #59645, #90574, #52024, #68244, #13942, #75839, #52520, #14439, #13443, #45411, #76334, #6829, #86457, #63643, #94063, #32165, #221, #38277, #56026, #46398, #23032, #69234, #46900, #32668, #39276, #94567, #70739, #93554, #25051, #15437, #7322, #716, #76824, #100152, #55019, #86955, #54027, #40288, #92561, #55524, #24551, #31163, #62635, #30671, #16943, #63138, #17442, #61641, #84951, #85957, #62133, #78825, #77328, #47905, #54515, #31665, #7829, #38778, #69740, #70236, #9325, #24048, #77823, #93058, #23536, #85448, #16434, #47403, #15934, #78331, #71242, #1728, #8331, #1231, #8835, #39772, #71744, #57030, #27065, #79338, #48409, #19441, #95571, #65652, #72749, #81350, #33678, #96564, #10841, #48912, #2238, #41805, #33169, #26058, #9832, #58029, #42313, #64150, #87966, #3247, #18447, #73244, #3738, #49419, #34181, #2739, #50406, #95074, #64657, #11337, #41289, #56528, #57531, #72247, #80345, #40785, #18941, #49921, #34679, #25559, #80852, #17949, #87460, #79838, #65157, #10336, #96076, #88968, #26571, #88466, #16771, #61963, #23367, #92889, #39612, #93898, #94401, #550, #48239, #47233, #78654, #47738, #62460, #39106, #24386, #54852, #17786, #24883, #54351, #16274, #55355, #78156, #55860, #86786, #8671, #86288, #93389, #38612, #70563, #63987, #48749, #77660, #62973, #94898, #79671, #9161, #1060, #85792, #40120, #71076, #40626, #1567, #69572, #87285, #51, #23877, #25390, #46734, #8167, #70063, #32001, #32506, #63479, #17278, #79171, #9671, #71579, #2073, #31496, #33012, #56367, #30996, #85280, #15769, #37321, #93080, #54534, #85469, #77845, #84479, #8351, #15459, #38300, #39300, #60666, #52541, #45933, #21569, #13963, #100175, #739, #68268, #15955, #53049, #46921, #44939, #61663, #7345, #75861, #69760, #7852, #70256, #31692, #62660, #30691, #6857, #23565, #83476, #241, #99682, #76843, #6364, #99196, #29696, #91589, #14459, #22068, #92088, #83980, #45439, #76354, #92580, #14960, #37810, #69257, #68762, #31184, #30186, #46419, #61168, #53549, #22557, #23059, #54048, #84974, #77350, #38799, #62157, #87987, #39800, #26078, #63668, #2757, #80370, #10353, #48930, #56047, #3264, #40802, #63157, #86476, #18464, #34203, #94588, #72269, #72770, #40310, #10860, #9850, #70758, #41824, #79859, #71765, #16453, #78351, #47424, #25069, #48428, #41310, #33698, #64676, #16962, #79358, #17464, #95093, #93575, #8852, #86972, #32185, #57051, #49436, #2257, #24071, #87479, #33190, #55040, #94084, #85978, #64172, #1256, #24569, #25578, #55546, #47926, #78847, #9347, #71259, #95591, #1749, #56551, #32687, #17971, #51422, #20949, #44314, #13334, #43314, #50424, #67159, #65174, #12837, #42820, #19956, #75240, #90474, #51921, #18963, #43806, #81865, #35199, #5732, #96101, #88987, #74252, #27588, #81367, #50927, #28574, #74740, #73264, #59038, #96586, #97090, #49941, #19457, #42331, #97583, #26589, #82850, #73751, #98067, #12344, #57549, #11850, #59534, #4746, #65670, #88488, #35697, #80871, #4250, #11358, #3758, #82358, #34699, #28085, #27084, #66171, #5237, #36195, #58539, #66672, #89479, #58051, #89976, #20450, #22925, #99065, #13833, #69127, #60542, #52920, #6726, #45797, #14330, #69639, #29563, #91457, #91963, #61032, #38167, #85346, #52418, #7728, #117, #44808, #46292, #92453, #54411, #30564, #14829, #76228, #84346, #37679, #92954, #83852, #21935, #76718, #15832, #83349, #31056, #68141, #62028, #29067, #7218, #84850, #100050, #23428, #30059, #22435, #46801, #61536, #68639, #53916, #99556, #15328, #77221, #45307, #53418, #77722, #36687, #67652, #90968, #38674, #75726, #98571, #60040, #21438, #6229, #37185, #24453, #2143, #78227, #47801, #8235, #93455, #70130, #39675, #40188, #62526, #63039, #85860, #40690, #86848, #48306, #63547, #71141, #2637, #54915, #41196, #78720, #17853, #95472, #25456, #64054, #32065, #8738, #39175, #72149, #56432, #56931, #71642, #33577, #23948, #70631, #1127, #618, #93961, #16336, #64555, #31563, #9224, #25959, #18350, #47302, #32566, #87864, #1634, #49318, #55926, #55420, #86359, #16843, #94469, #24952, #87353, #17345, #79236, #9735, #33077, #94967, #48814, #79739, #10234, #96972, #4130, #28446, #57933, #27472, #88873, #97469, #27959, #50310, #66052, #34584, #97950, #41706, #65555, #66558, #42214, #57435, #12220, #3636, #42704, #90356, #58429, #49824, #50808, #82239, #89361, #10742, #59409, #20829, #96469, #67042, #19829, #88364, #80248, #35583, #81747, #3143, #65056, #34084, #81245, #35080, #58915, #89858, #26959, #43198, #74137, #4630, #72648, #95973, #51299, #12718, #18843, #20325, #43686, #26472, #74625, #5118, #19343, #36070, #11727, #80756, #73639, #73147, #11237, #30951, #98451, #15226, #83237, #84737, #44190, #91849, #99943, #53301, #77112, #45191, #37569, #46184, #45686, #52801, #69018, #91350, #84233, #14719, #29445, #6617, #61917, #7619, #38569, #5618, #44690, #90854, #69526, #92844, #75610, #51805, #8, #68031, #76609, #21325, #21825, #82736, #36560, #13218, #13720, #83735, #67531, #6115, #28953, #7114, #29952, #22323, #68521, #14215, #75125, #59925, #52301, #76116, #61420, #37066, #30456, #38062, #98957, #60425, #99452, #60920, #92346, #22819, #53803, #48705, #23325, #62931, #79627, #33454, #62419, #47692, #10119, #2524, #40076, #93851, #70522, #1519, #94351, #25343, #24344, #2025, #64444, #1012, #54310, #17230, #31453, #93342, #54807, #31958, #71030, #78611, #39571, #55311, #32458, #86244, #56321, #85745, #32967, #16725, #9117, #24840, #72038, #39065, #94853, #87241, #23834, #63944, #79127, #41083, #48195, #63434, #55814, #86742, #9621, #85236, #40582, #16228, #17737, #47193, #70015, #15725, #78110, #46694, #77614, #71533, #8125, #502, #8623, #88758, #81134, #27844, #89249, #96360, #12110, #34466, #96859, #27351, #35958, #19229, #74516, #20220, #51191, #49206, #88253, #33961, #82132, #5008, #18727, #95359, #12618, #11121, #19717, #64941, #65441, #25843, #80134, #56820, #66438, #26849, #10626, #49706, #72532, #58312, #73527, #34964, #50193, #57816, #89750, #41588, #58800, #11613, #4521, #43577, #43083, #50690, #80636, #95857, #42590, #42090, #74026, #87752, #81637, #18236, #3026, #26349, #57324, #73036, #3521, #35469, #97362, #4018, #65937, #21219, #84624, #28340, #52188, #53194, #28849, #44073, #22707, #46079, #83624, #36955, #13607, #45082, #37462, #68904, #76003, #97846, #15114, #7501, #83117, #53696, #14106, #75006, #76998, #22211, #6510, #90246, #44574, #67923, #68410, #75503, #99829, #59812, #76498, #6003, #99343, #29841, #59302, #66927, #84124, #29340, #5504, #30336, #20721, #60310, #51691, #60809, #98844, #91733, #91238, #82624, #21711, #90745, #45581, #67421, #13107, #14610, #61310, #36453, #7005, #37952, #52685, #92234, #98342, #86628, #24720, #94737, #32341, #39459, #55701, #77996, #39956, #70917, #79515, #31850, #17620, #38950, #390, #48592, #62818, #17113, #55199, #8508, #38453, #87128, #62306, #47582, #23721, #24227, #1905, #48081, #46574, #63317, #69905, #70409, #92727, #93231, #15609, #1407, #16605, #78501, #93732, #895, #32848, #85123, #71414, #86129, #9003, #31340, #61807, #94235, #30841, #79007, #69408, #63824, #9505, #100325, #40465, #25224, #56202, #23214, #54199, #77500, #8002, #54691, #85626, #16110, #47081, #33335, #97601, #2406, #50946, #10004, #44331, #28594, #60060, #43824, #5753, #64327, #81387, #73769, #40962, #66189, #95244, #36707, #71922, #81884, #98088, #4268, #89003, #74759, #35217, #74271, #21458, #59059, #11868, #97110, #67673, #52437, #12360, #90492, #90987, #58556, #25731, #5254, #19476, #50440, #67176, #89996, #58070, #42839, #27607, #43333, #66690, #59556, #20968, #51939, #89495, #28101, #35717, #12856, #19977, #4763, #82868, #75260, #20469, #13355, #51440, #98593, #36212, #82377, #29086, #21956, #13857, #7239, #83368, #75749, #61555, #62548, #29584, #46822, #14350, #15850, #6250, #22948, #31076, #84869, #62048, #69658, #39192, #93472, #31583, #92473, #68659, #85365, #44827, #92974, #61051, #38189, #23965, #8254, #70148, #37207, #76249, #52939, #635, #68159, #99085, #6745, #53938, #45816, #99576, #69147, #77738, #23449, #91479, #77239, #45328, #14851, #60561, #37699, #83870, #15350, #46314, #7746, #38692, #30082, #53440, #54432, #91983, #22454, #84370, #135, #76737, #100068, #30584, #63565, #71660, #79254, #71160, #24969, #64071, #32585, #87882, #16860, #64572, #94485, #9751, #56449, #3160, #70654, #25977, #18366, #63058, #95491, #10251, #72663, #48832, #33092, #55943, #2159, #86869, #10760, #1650, #47819, #33592, #55437, #1145, #49334, #86376, #80266, #47322, #94986, #2657, #87374, #41723, #48326, #40706, #34102, #79758, #17364, #72166, #25472, #17868, #41214, #95991, #56948, #65074, #54934, #85877, #8755, #78743, #93979, #16354, #78244, #9243, #39694, #32082, #24471, #40205, #96487, #66069, #26488, #11254, #88381, #97967, #27488, #80772, #81262, #3655, #58932, #4647, #66573, #81765, #58445, #20847, #73164, #59432, #96989, #36090, #13236, #43705, #82258, #50326, #26978, #12235, #42723, #74642, #75142, #89875, #51824, #42230, #57949, #88888, #57452, #11746, #34600, #82753, #18862, #89378, #44210, #36579, #65572, #50824, #5633, #67551, #43216, #74154, #19361, #35602, #19848, #73655, #97486, #27979, #28467, #20345, #49839, #4148, #35101, #51318, #12735, #5136, #67058, #90372, #53823, #76628, #21342, #52320, #99468, #53322, #84755, #15242, #46199, #21842, #84252, #22338, #99962, #46710, #13735, #69545, #30968, #6132, #7639, #77130, #15744, #92365, #7129, #77632, #37085, #28969, #14737, #98469, #90871, #38079, #8144, #44706, #61935, #29462, #92865, #83254, #69034, #38585, #30472, #23341, #91867, #45703, #54326, #39081, #61438, #83752, #25, #59943, #85251, #76135, #22836, #75631, #68048, #98972, #60445, #91366, #52817, #14232, #45208, #6632, #37586, #68538, #29967, #60936, #55830, #33470, #79641, #78127, #63959, #1026, #1535, #23852, #24361, #47208, #2043, #48214, #9639, #24856, #32475, #64461, #16247, #2538, #40091, #86757, #70539, #93360, #17246, #62434, #9133, #70035, #95375, #87258, #18251, #32984, #25863, #54826, #39587, #31977, #523, #55327, #85762, #56836, #31473, #86261, #56338, #62945, #8642, #94868, #93869, #79141, #16741, #47709, #40599, #78626, #71046, #63450, #87769, #17752, #49223, #25358, #80152, #94369, #71549, #48723, #10136, #41101, #72054, #10641, #3040, #26864, #27860, #3539, #18742, #74041, #65457, #4034, #51704, #89264, #11138, #34480, #35972, #82639, #11629, #90260, #41603, #57832, #28354, #58327, #49720, #20736, #97376, #19732, #64960, #26366, #95871, #42607, #96876, #58815, #89765, #20236, #96374, #27365, #65953, #33978, #72548, #51204, #34978, #80653, #74533, #97859, #50705, #59317, #35485, #81655, #57339, #42108, #88269, #12124, #73054, #88774, #43098, #19242, #50209, #5023, #81151, #82146, #12632, #73542, #4538, #66456, #43592, #66942, #69424, #92747, #61824, #91746, #98860, #15130, #13122, #61327, #91254, #68425, #23230, #75517, #54216, #6524, #92251, #29855, #83639, #44089, #75018, #36972, #22226, #76020, #29354, #99359, #77016, #22723, #21232, #7020, #44589, #45099, #67433, #37475, #100342, #5516, #36467, #30858, #21727, #46093, #60825, #98358, #60329, #7518, #28863, #14121, #53209, #68920, #99845, #30353, #67937, #84137, #14627, #59825, #90758, #53713, #45594, #52204, #38472, #83131, #76514, #13619, #37969, #84640, #6017, #52700, #15627, #9024, #85140, #77519, #63337, #64344, #31360, #48609, #408, #63842, #32868, #39476, #70936, #8019, #94755, #71434, #40983, #95262, #33355, #94254, #70429, #87148, #46595, #25244, #62836, #39972, #25752, #47098, #38969, #78517, #56218, #1424, #55218, #69922, #62324, #8526, #24739, #47600, #914, #32359, #79534, #17637, #93252, #79025, #16128, #16628, #23739, #54712, #17131, #55719, #86646, #48100, #9523, #10022, #85649, #71941, #86146, #2423, #78014, #1925, #40481, #31867, #93753, #24246, #72935, #35862, #12020, #89154, #51093, #10522, #26254, #18628, #87656, #11028, #41483, #82037, #56721, #96266, #12517, #66834, #95760, #81040, #43484, #97755, #73433, #26751, #3435, #49605, #74424, #18137, #57716, #35374, #49106, #34368, #80037, #50590, #64850, #57226, #88158, #65349, #3930, #11518, #88658, #42989, #19128, #80535, #89649, #73927, #4916, #81546, #34867, #50100, #65838, #42498, #72438, #96760, #41998, #66336, #27258, #2931, #58213, #20131, #33864, #97260, #4423, #19628, #27751, #58701, #21612, #14006, #61213, #22114, #29239, #45484, #67825, #29743, #60710, #69302, #52583, #7392, #28748, #90641, #38349, #83520, #6902, #44981, #98748, #52089, #28246, #53598, #44478, #53096, #98243, #60209, #59207, #13008, #90149, #99728, #91138, #75906, #75403, #6411, #84522, #20625, #51592, #45976, #5903, #22604, #74905, #92133, #37367, #37855, #15009, #76399, #84022, #83017, #59710, #68310, #36861, #82527, #14509, #43973, #99241, #91630, #68809, #30232, #76890, #13506, #5410, #36362, #67318, #21118, #25115, #9898, #38847, #24119, #56091, #79407, #16499, #70308, #46971, #78398, #70810, #1799, #8901, #30739, #48481, #77893, #40850, #94129, #7896, #69805, #31235, #8398, #47471, #55089, #16002, #788, #39847, #39349, #32735, #62203, #9396, #31740, #1299, #32232, #61705, #86023, #285, #23107, #63207, #92629, #62708, #100221, #63719, #17008, #54095, #24613, #94635, #85016, #93126, #23608, #15500, #54582, #46467, #87024, #77396, #85518, #86522, #93623, #55593, #47973, #78898, #40357, #71311, #17514, #41357, #64726, #66217, #12391, #41871, #50469, #50976, #18511, #81913, #65717, #79910, #20009, #27133, #49987, #95142, #56600, #25628, #72815, #26635, #58097, #89033, #19508, #95643, #57596, #96148, #73311, #71815, #87534, #42868, #4297, #10399, #27637, #34249, #2808, #80914, #10908, #19008, #3318, #58582, #88036, #33745, #81418, #72311, #33236, #11405, #35248, #18014, #11899, #73799, #26128, #88532, #97137, #65224, #42379, #89525, #96631, #3806, #2305, #34744, #64216, #48977, #57099, #49484, #80414, #43856, #5283, #53472, #36736, #21986, #60090, #13382, #67205, #85780, #68688, #59588, #37237, #12884, #82897, #43364, #28132, #4792, #14380, #44362, #75286, #90518, #5781, #99606, #35747, #74301, #61082, #20996, #91015, #22482, #51969, #6772, #67704, #37727, #90026, #76278, #98621, #52967, #30109, #60591, #99115, #98118, #74785, #29115, #21487, #66718, #29612, #97628, #92011, #59089, #36244, #28624, #20498, #52466, #51470, #82404, #83398, #13883, #44857, #75780, #6279, #68188, #91507, #83902, #45356, #63465, #40106, #9657, #33489, #49240, #94387, #79657, #18268, #71063, #16262, #25375, #24374, #55343, #16755, #24869, #40612, #17263, #1552, #55845, #71567, #32493, #2553, #47725, #78641, #48227, #79157, #63974, #47220, #31989, #64477, #95391, #86275, #1045, #9147, #39599, #86773, #2060, #32999, #94884, #56353, #56852, #87272, #17772, #48737, #78142, #93886, #25881, #10157, #87785, #70551, #41116, #72073, #8657, #62958, #100297, #92700, #39431, #363, #7467, #23690, #46054, #7973, #38925, #84599, #61780, #86100, #31822, #62791, #59396, #98438, #44176, #93706, #16579, #30307, #47554, #24197, #22682, #31311, #75109, #76973, #5105, #90343, #67030, #36549, #38427, #20816, #61285, #82724, #69879, #85096, #46544, #23188, #36055, #69378, #85595, #97938, #53668, #28433, #62280, #13200, #5605, #67517, #15087, #51789, #92208, #30815, #54174, #15580, #93205, #54665, #16082, #77474, #47052, #77966, #8481, #55173, #70380, #870, #10982, #86600, #32315, #78980, #70891, #9477, #95219, #96225, #17087, #8976, #2378, #78475, #1382, #56676, #57668, #24692, #41947, #40438, #72890, #63288, #18093, #26206, #79987, #3388, #71893, #34323, #88611, #26708, #87610, #63797, #80487, #39928, #57180, #56172, #33309, #19083, #65301, #94205, #55674, #71390, #48050, #1873, #32820, #94712, #25196, #49059, #40932, #87100, #64296, #17592, #88114, #48564, #72392, #79490, #9977, #25700, #10475, #41435, #2887, #33817, #64802, #95718, #18581, #49558, #96709, #66288, #13465, #4871, #50543, #73390, #35819, #42450, #89605, #50055, #82974, #67279, #98703, #82482, #44437, #3884, #19583, #11977, #80994, #4379, #34823, #67786, #11476, #35327, #36320, #42945, #27212, #12963, #73881, #12475, #60170, #97711, #81498, #97215, #75361, #65794, #29201, #91092, #27710, #36818, #66792, #89110, #58656, #20084, #28204, #74374, #51052, #81991, #59161, #43444, #5861, #90105, #59668, #20579, #51552, #43931, #58167, #74862, #98197, #5366, #28707, #90598, #21077, #52044, #33293, #1857, #2871, #24179, #16062, #9461, #85579, #77951, #63780, #64786, #31805, #49043, #16561, #18074, #8464, #25179, #64279, #10459, #78961, #71375, #79971, #79472, #86583, #2362, #24674, #87084, #17573, #26189, #40419, #95701, #86082, #47536, #47035, #32801, #95202, #94696, #55656, #8960, #39414, #41419, #1364, #9963, #55155, #17069, #70364, #849, #62774, #56656, #48035, #56155, #32298, #48545, #72376, #93690, #78459, #33803, #63271, #39908, #70874, #94188, #40913, #25685, #71876, #87594, #12455, #80975, #57653, #42927, #73370, #36304, #43426, #10967, #34806, #73863, #65779, #74358, #4851, #11462, #41932, #82467, #57162, #96693, #12945, #67263, #96209, #81482, #43915, #98183, #4363, #27196, #3868, #35311, #27695, #59146, #66273, #89091, #72874, #19568, #74845, #18568, #88100, #5349, #58151, #90086, #97196, #49543, #50526, #20562, #11956, #88596, #80472, #58640, #3375, #89588, #34306, #51532, #35803, #65285, #20069, #51032, #81975, #66776, #97693, #28189, #26694, #42435, #19068, #50042, #13946, #14940, #91075, #5845, #61148, #52524, #91570, #38783, #76337, #6834, #99664, #30675, #37793, #59650, #77333, #69744, #44922, #15441, #45415, #36800, #7833, #84457, #68746, #52028, #13447, #82956, #29679, #83963, #45913, #21552, #38282, #37302, #30169, #92071, #90580, #28685, #76827, #22051, #67762, #61646, #21058, #6342, #44422, #7327, #22542, #46401, #98684, #75344, #53033, #83458, #69238, #29178, #60154, #53533, #92564, #75845, #100156, #23036, #68249, #14443, #99177, #54030, #84955, #60650, #79842, #48915, #78828, #85962, #2241, #32673, #41292, #94068, #10340, #719, #62639, #225, #24554, #79342, #16948, #70742, #31166, #62136, #24052, #9329, #63142, #16438, #86460, #64153, #9836, #93061, #71748, #1237, #23541, #47406, #54519, #94571, #8335, #39281, #31669, #8838, #47908, #55528, #78335, #32169, #40292, #39776, #33173, #93558, #40789, #71245, #1734, #63646, #85451, #15938, #95078, #25562, #70240, #56532, #25054, #46904, #55023, #56030, #86958, #17445, #48412, #87463, #17954, #77828, #52278, #52781, #18451, #37047, #3250, #6094, #64662, #13193, #21307, #75101, #98938, #65655, #58033, #68007, #67509, #73247, #90834, #11342, #5598, #36542, #14195, #27070, #83717, #29425, #60407, #26063, #65160, #10845, #91328, #72251, #96081, #2742, #21804, #88470, #98430, #41808, #42317, #33682, #57034, #95574, #44672, #3741, #87969, #26574, #49423, #28934, #51781, #44168, #90333, #34683, #80348, #72754, #34185, #96568, #83214, #57536, #13697, #59903, #18944, #49925, #20809, #80856, #75591, #82716, #22797, #61897, #53783, #62392, #93323, #15204, #30929, #99920, #62908, #6596, #30431, #31433, #7094, #22303, #77592, #68996, #7593, #46164, #92324, #23304, #15705, #47170, #54289, #76095, #68500, #77094, #100418, #479, #23813, #54786, #61401, #92822, #69501, #46669, #93831, #60900, #16203, #84209, #78089, #37549, #84713, #91826, #85721, #85217, #24317, #14700, #99434, #8096, #45173, #29929, #39045, #55290, #53281, #8601, #76590, #39548, #45665, #38545, #69993, #38043, #70500, #989, #31938, #86220, #65415, #95333, #1994, #18693, #16703, #64915, #94828, #72012, #96330, #42063, #73008, #71007, #9597, #33431, #87216, #26818, #57783, #40557, #25821, #79604, #32940, #2493, #80602, #26323, #24811, #10592, #48170, #48680, #1497, #71509, #94326, #49181, #56793, #34436, #25318, #49675, #64416, #47671, #63914, #11094, #87727, #17205, #40049, #18209, #9095, #56294, #78585, #3495, #33936, #32434, #80105, #63408, #55792, #95828, #57297, #17710, #41559, #10094, #86715, #79098, #41053, #3000, #72507, #88229, #20690, #12079, #51156, #98814, #35926, #58282, #81608, #83083, #29308, #19196, #36922, #88727, #73999, #75468, #4979, #65910, #67891, #44041, #66897, #11585, #73494, #43052, #89221, #74486, #4492, #50167, #74972, #42562, #66408, #3989, #19689, #50660, #81104, #35439, #34932, #13574, #96825, #27816, #44543, #27321, #97328, #12586, #5972, #58769, #97819, #89721, #20191, #28312, #59268, #82105, #43549, #67387, #90216, #51661, #82598, #13074, #5475, #36423, #98311, #28814, #59780, #90713, #21188, #52154, #69372, #37923, #93199, #22180, #69874, #15081, #84592, #61775, #8475, #75970, #31305, #23685, #68380, #54659, #38421, #91204, #99313, #100292, #99795, #7462, #30302, #16076, #76469, #53163, #38920, #39425, #6478, #85589, #91696, #47046, #52651, #30810, #7967, #92694, #77961, #53663, #46048, #70375, #54168, #61279, #77467, #92202, #23181, #85090, #864, #76967, #60281, #21679, #83587, #14074, #84092, #29806, #45051, #37430, #14578, #60777, #45548, #6974, #15575, #68871, #22677, #46539, #357, #62274, #2882, #63791, #86095, #86595, #8970, #64291, #9972, #71888, #87095, #94707, #26201, #78470, #64796, #1868, #41428, #18577, #49053, #87605 ),
 .UNSPECIFIED., .F., .F.,
 ( 4, 2, 2, 2, 2, 2, 2, 2, 2, 2, 2, 2, 2, 2, 2, 2, 2, 2, 2, 2, 2, 2, 2, 2, 2, 2, 2, 2, 2, 2, 2, 2, 2, 2, 2, 2, 2, 2, 2, 2, 2, 2, 2, 2, 2, 2, 2, 2, 2, 2, 2, 2, 2, 2, 2, 2, 2, 2, 2, 2, 2, 2, 2, 2, 2, 2, 2, 2, 2, 2, 2, 2, 2, 2, 2, 2, 2, 2, 2, 2, 2, 2, 2, 2, 2, 2, 2, 2, 2, 2, 2, 2, 2, 2, 2, 2, 2, 2, 2, 2, 2, 2, 2, 2, 2, 2, 2, 2, 2, 2, 2, 2, 2, 2, 2, 2, 2, 2, 2, 2, 2, 2, 2, 2, 2, 2, 2, 2, 2, 2, 2, 2, 2, 2, 2, 2, 2, 2, 2, 2, 2, 2, 2, 2, 2, 2, 2, 2, 2, 2, 2, 2, 2, 2, 2, 2, 2, 2, 2, 2, 2, 2, 2, 2, 2, 2, 2, 2, 2, 2, 2, 2, 2, 2, 2, 2, 2, 2, 2, 2, 2, 2, 2, 2, 2, 2, 2, 2, 2, 2, 2, 2, 2, 2, 2, 2, 2, 2, 2, 2, 2, 2, 2, 2, 2, 2, 2, 2, 2, 2, 2, 2, 2, 2, 2, 2, 2, 2, 2, 2, 2, 2, 2, 2, 2, 2, 2, 2, 2, 2, 2, 2, 2, 2, 2, 2, 2, 2, 2, 2, 2, 2, 2, 2, 2, 2, 2, 2, 2, 2, 2, 2, 2, 2, 2, 2, 2, 2, 2, 2, 2, 2, 2, 2, 2, 2, 2, 2, 2, 2, 2, 2, 2, 2, 2, 2, 2, 2, 2, 2, 2, 2, 2, 2, 2, 2, 2, 2, 2, 2, 2, 2, 2, 2, 2, 2, 2, 2, 2, 2, 2, 2, 2, 2, 2, 2, 2, 2, 2, 2, 2, 2, 2, 2, 2, 2, 2, 2, 2, 2, 2, 2, 2, 2, 2, 2, 2, 2, 2, 2, 2, 2, 2, 2, 2, 2, 2, 2, 2, 2, 2, 2, 2, 2, 2, 2, 2, 2, 2, 2, 2, 2, 2, 2, 2, 2, 2, 2, 2, 2, 2, 2, 2, 2, 2, 2, 2, 2, 2, 2, 2, 2, 2, 2, 2, 2, 2, 2, 2, 2, 2, 2, 2, 2, 2, 2, 2, 2, 2, 2, 2, 2, 2, 2, 2, 2, 2, 2, 2, 2, 2, 2, 2, 2, 2, 2, 2, 2, 2, 2, 2, 2, 2, 2, 2, 2, 2, 2, 2, 2, 2, 2, 2, 2, 2, 2, 2, 2, 2, 2, 2, 2, 2, 2, 2, 2, 2, 2, 2, 2, 2, 2, 2, 2, 2, 2, 2, 2, 2, 2, 2, 2, 2, 2, 2, 2, 2, 2, 2, 2, 2, 2, 2, 2, 2, 2, 2, 2, 2, 2, 2, 2, 2, 2, 2, 2, 2, 2, 2, 2, 2, 2, 2, 2, 2, 2, 2, 2, 2, 2, 2, 2, 2, 2, 2, 2, 2, 2, 2, 2, 2, 2, 2, 2, 2, 2, 2, 2, 2, 2, 2, 2, 2, 2, 2, 2, 2, 2, 2, 2, 2, 2, 2, 2, 2, 2, 2, 2, 2, 2, 2, 2, 2, 2, 2, 2, 2, 2, 2, 2, 2, 2, 2, 2, 2, 2, 2, 2, 2, 2, 2, 2, 2, 2, 2, 2, 2, 2, 2, 2, 2, 2, 2, 2, 2, 2, 2, 2, 2, 2, 2, 2, 2, 2, 2, 2, 2, 2, 2, 2, 2, 2, 2, 2, 2, 2, 2, 2, 2, 2, 2, 2, 2, 2, 2, 2, 2, 2, 2, 2, 2, 2, 2, 2, 2, 2, 2, 2, 2, 2, 2, 2, 2, 2, 2, 2, 2, 2, 2, 2, 2, 2, 2, 2, 2, 2, 2, 2, 2, 2, 2, 2, 2, 2, 2, 2, 2, 2, 2, 2, 2, 2, 2, 2, 2, 2, 2, 2, 2, 2, 2, 2, 2, 2, 2, 2, 2, 2, 2, 2, 2, 2, 2, 2, 2, 2, 2, 2, 2, 2, 2, 2, 2, 2, 2, 2, 2, 2, 2, 2, 2, 2, 2, 2, 2, 2, 2, 2, 2, 2, 2, 2, 2, 2, 2, 2, 2, 2, 2, 2, 2, 2, 2, 2, 2, 2, 2, 2, 2, 2, 2, 2, 2, 2, 2, 2, 2, 2, 2, 2, 2, 2, 2, 2, 2, 2, 2, 2, 2, 2, 2, 2, 2, 2, 2, 2, 2, 2, 2, 2, 2, 2, 2, 2, 2, 2, 2, 2, 2, 2, 2, 2, 2, 2, 2, 2, 2, 2, 2, 2, 2, 2, 2, 2, 2, 2, 2, 2, 2, 2, 2, 2, 2, 2, 2, 2, 2, 2, 2, 2, 2, 2, 2, 2, 2, 2, 2, 2, 2, 2, 2, 2, 2, 2, 2, 2, 2, 2, 2, 2, 2, 2, 2, 2, 2, 2, 2, 2, 2, 2, 2, 2, 2, 2, 2, 2, 2, 2, 2, 2, 2, 2, 2, 2, 2, 2, 2, 2, 2, 2, 2, 2, 2, 2, 2, 2, 2, 2, 2, 2, 2, 2, 2, 2, 2, 2, 2, 2, 2, 2, 2, 2, 2, 2, 2, 2, 2, 2, 2, 2, 2, 2, 2, 2, 2, 2, 2, 2, 2, 2, 2, 2, 2, 2, 2, 2, 2, 2, 2, 2, 2, 2, 2, 2, 2, 2, 2, 2, 2, 2, 2, 2, 2, 2, 2, 2, 2, 2, 2, 2, 2, 2, 2, 2, 2, 2, 2, 2, 2, 2, 2, 2, 2, 2, 2, 2, 2, 2, 2, 2, 2, 2, 2, 2, 2, 2, 2, 2, 2, 2, 2, 2, 2, 2, 2, 2, 2, 2, 2, 2, 2, 2, 2, 2, 2, 2, 2, 2, 2, 2, 2, 2, 2, 2, 2, 2, 2, 2, 2, 2, 2, 2, 2, 2, 2, 2, 2, 2, 2, 2, 2, 2, 2, 2, 2, 2, 2, 2, 2, 2, 2, 2, 2, 2, 2, 2, 2, 2, 2, 2, 2, 2, 2, 2, 2, 2, 2, 2, 2, 2, 2, 2, 2, 2, 2, 2, 2, 2, 2, 2, 2, 2, 2, 2, 2, 2, 2, 2, 2, 2, 2, 2, 2, 2, 2, 2, 2, 2, 2, 2, 2, 2, 2, 2, 2, 2, 2, 2, 2, 2, 2, 2, 2, 2, 2, 2, 2, 2, 2, 2, 2, 2, 2, 2, 2, 2, 2, 2, 2, 2, 2, 2, 2, 2, 2, 2, 2, 2, 2, 2, 2, 2, 2, 2, 2, 2, 2, 2, 2, 2, 2, 2, 2, 2, 2, 2, 2, 2, 2, 2, 2, 2, 2, 2, 2, 2, 2, 2, 2, 2, 2, 2, 2, 2, 2, 2, 2, 2, 2, 2, 2, 2, 2, 2, 2, 2, 2, 2, 2, 2, 2, 2, 2, 2, 2, 2, 2, 2, 2, 2, 2, 2, 2, 2, 2, 2, 2, 2, 2, 2, 2, 2, 2, 2, 2, 2, 2, 2, 2, 2, 2, 2, 2, 2, 2, 2, 2, 2, 2, 2, 2, 2, 2, 2, 2, 2, 2, 2, 2, 2, 2, 2, 2, 2, 2, 2, 2, 2, 2, 2, 2, 2, 2, 2, 2, 2, 2, 2, 2, 2, 2, 2, 2, 2, 2, 2, 2, 2, 2, 2, 2, 2, 2, 2, 2, 2, 2, 2, 2, 2, 2, 2, 2, 2, 2, 2, 2, 2, 2, 2, 2, 2, 2, 2, 2, 2, 2, 2, 2, 2, 2, 2, 2, 2, 2, 2, 2, 2, 2, 2, 2, 2, 2, 2, 2, 2, 2, 2, 2, 2, 2, 2, 2, 2, 2, 2, 2, 2, 2, 2, 2, 2, 2, 2, 2, 2, 2, 2, 2, 2, 2, 2, 2, 2, 2, 2, 2, 2, 2, 2, 2, 2, 2, 2, 2, 2, 2, 2, 2, 2, 2, 2, 2, 2, 2, 2, 2, 2, 2, 2, 2, 2, 2, 2, 2, 2, 2, 2, 2, 2, 2, 2, 2, 2, 2, 2, 2, 2, 2, 2, 2, 2, 2, 2, 2, 2, 2, 2, 2, 2, 2, 2, 2, 2, 2, 2, 2, 2, 2, 2, 2, 2, 2, 2, 2, 2, 2, 2, 2, 2, 2, 2, 2, 2, 2, 2, 2, 2, 2, 2, 2, 2, 2, 2, 2, 2, 2, 2, 2, 2, 2, 2, 2, 2, 2, 2, 2, 2, 2, 2, 2, 2, 2, 2, 2, 2, 2, 2, 2, 2, 2, 2, 2, 2, 2, 2, 2, 2, 2, 2, 2, 2, 2, 2, 2, 2, 2, 2, 2, 2, 2, 2, 2, 2, 2, 2, 2, 2, 2, 2, 2, 2, 2, 2, 2, 2, 2, 2, 2, 2, 2, 2, 2, 2, 2, 2, 2, 2, 2, 2, 2, 2, 2, 2, 2, 2, 2, 2, 2, 2, 2, 2, 2, 2, 2, 2, 2, 2, 2, 2, 2, 2, 2, 2, 2, 2, 2, 2, 2, 2, 2, 2, 2, 2, 2, 2, 2, 2, 2, 2, 2, 2, 2, 2, 2, 2, 2, 2, 2, 2, 2, 2, 2, 2, 2, 2, 2, 2, 2, 2, 2, 2, 2, 2, 2, 2, 2, 2, 2, 2, 2, 2, 2, 2, 2, 2, 2, 2, 2, 2, 2, 2, 2, 2, 2, 2, 2, 2, 2, 2, 2, 2, 2, 2, 2, 2, 2, 2, 2, 2, 2, 2, 2, 2, 2, 2, 2, 2, 2, 2, 2, 2, 2, 2, 2, 2, 2, 2, 2, 2, 2, 2, 2, 2, 2, 2, 2, 2, 2, 2, 2, 2, 2, 2, 2, 2, 2, 2, 2, 2, 2, 2, 2, 2, 2, 2, 2, 2, 2, 2, 2, 2, 2, 2, 2, 2, 2, 2, 2, 2, 2, 2, 2, 2, 2, 2, 2, 2, 2, 2, 2, 2, 2, 2, 2, 2, 2, 2, 2, 2, 2, 2, 2, 2, 2, 2, 2, 2, 2, 2, 2, 2, 2, 2, 2, 2, 2, 2, 2, 2, 2, 2, 2, 2, 2, 2, 2, 2, 2, 2, 2, 2, 2, 2, 2, 2, 2, 2, 2, 2, 2, 2, 2, 2, 2, 2, 2, 2, 2, 2, 2, 2, 2, 2, 2, 2, 2, 2, 2, 2, 2, 2, 2, 2, 2, 2, 2, 2, 2, 2, 2, 2, 2, 2, 2, 2, 2, 2, 2, 2, 2, 2, 2, 2, 2, 2, 2, 2, 2, 2, 2, 2, 2, 2, 2, 2, 2, 2, 2, 2, 2, 2, 2, 2, 2, 2, 2, 2, 2, 2, 2, 2, 2, 2, 2, 2, 2, 2, 2, 2, 2, 2, 2, 2, 2, 2, 2, 2, 2, 2, 2, 2, 2, 2, 2, 2, 2, 2, 2, 2, 2, 2, 2, 2, 2, 2, 2, 2, 2, 2, 2, 2, 2, 2, 2, 2, 2, 2, 2, 2, 2, 2, 2, 2, 2, 2, 2, 2, 2, 2, 2, 2, 2, 2, 2, 2, 2, 2, 2, 2, 2, 2, 2, 2, 2, 2, 2, 2, 2, 2, 2, 2, 2, 2, 2, 2, 2, 2, 2, 2, 2, 2, 2, 2, 2, 2, 2, 2, 2, 2, 2, 2, 2, 2, 2, 2, 2, 2, 2, 2, 2, 2, 2, 2, 2, 2, 2, 2, 2, 2, 2, 2, 2, 2, 2, 2, 2, 2, 2, 2, 2, 2, 2, 2, 2, 2, 2, 2, 2, 2, 2, 2, 2, 2, 2, 2, 2, 2, 2, 2, 2, 2, 2, 2, 2, 2, 2, 2, 2, 2, 2, 2, 2, 2, 2, 2, 2, 2, 2, 2, 2, 2, 2, 2, 2, 2, 2, 2, 2, 2, 2, 2, 2, 2, 2, 2, 2, 2, 2, 2, 2, 2, 2, 2, 2, 2, 2, 2, 2, 2, 2, 2, 2, 2, 2, 2, 2, 2, 2, 2, 2, 2, 2, 2, 2, 2, 2, 2, 2, 2, 2, 2, 2, 2, 2, 2, 2, 2, 2, 2, 2, 2, 2, 2, 2, 2, 2, 2, 2, 2, 2, 2, 2, 2, 2, 2, 2, 2, 2, 2, 2, 2, 2, 2, 2, 2, 2, 2, 2, 2, 2, 2, 2, 2, 2, 2, 2, 2, 2, 2, 2, 2, 2, 2, 2, 2, 2, 2, 2, 2, 2, 2, 2, 2, 2, 2, 2, 2, 2, 2, 2, 2, 2, 2, 2, 2, 2, 2, 2, 2, 2, 2, 2, 2, 2, 2, 2, 2, 2, 2, 2, 2, 2, 2, 2, 2, 2, 2, 4 ),
 ( 0.000000000000000000, 0.0004882812500000001084, 0.0009765625000000002168, 0.001464843750000000434, 0.001953125000000000000, 0.002441406250000000000, 0.002929687499999999566, 0.003417968749999999566, 0.003906249999999999133, 0.004394531249999998265, 0.004882812499999997398, 0.005371093749999997398, 0.005859374999999997398, 0.006347656249999998265, 0.006835937499999998265, 0.007324218749999998265, 0.007812499999999998265, 0.008300781249999998265, 0.008789062499999998265, 0.009277343749999998265, 0.009765624999999998265, 0.01025390624999999827, 0.01074218749999999827, 0.01123046874999999827, 0.01171874999999999827, 0.01220703125000000000, 0.01269531250000000000, 0.01318359375000000000, 0.01367187500000000000, 0.01416015625000000000, 0.01464843750000000000, 0.01513671875000000000, 0.01562500000000000000, 0.01611328125000000000, 0.01660156250000000000, 0.01708984375000000000, 0.01757812500000000000, 0.01806640625000000000, 0.01855468750000000000, 0.01904296875000000000, 0.01953125000000000000, 0.02001953125000000000, 0.02050781250000000000, 0.02099609375000000000, 0.02148437500000000000, 0.02197265625000000000, 0.02246093750000000000, 0.02294921875000000000, 0.02343750000000000000, 0.02392578125000000347, 0.02441406250000000347, 0.02490234375000000347, 0.02539062500000000347, 0.02587890625000000347, 0.02636718750000000347, 0.02685546875000000347, 0.02734375000000000347, 0.02783203125000000347, 0.02832031250000000347, 0.02880859375000000347, 0.02929687500000000347, 0.02978515625000000347, 0.03027343750000000347, 0.03076171875000000347, 0.03125000000000000000, 0.03173828125000000000, 0.03222656250000000000, 0.03271484375000000000, 0.03320312500000000000, 0.03369140625000000000, 0.03417968750000000000, 0.03466796875000000000, 0.03515625000000000000, 0.03564453125000000000, 0.03613281250000000000, 0.03662109375000000000, 0.03710937500000000000, 0.03759765625000000000, 0.03808593750000000000, 0.03857421875000000000, 0.03906250000000000000, 0.03955078125000000000, 0.04003906250000000000, 0.04052734375000000000, 0.04101562500000000000, 0.04150390625000000000, 0.04199218750000000000, 0.04248046875000000000, 0.04296875000000000000, 0.04345703125000000000, 0.04394531250000000000, 0.04443359375000000000, 0.04492187500000000000, 0.04541015625000000000, 0.04589843750000000000, 0.04638671875000000000, 0.04687500000000000000, 0.04736328125000000694, 0.04785156250000000694, 0.04833984375000000694, 0.04882812500000000694, 0.04931640625000000694, 0.04980468750000000694, 0.05029296875000000694, 0.05078125000000000694, 0.05126953125000000694, 0.05175781250000000694, 0.05224609375000000694, 0.05273437500000000694, 0.05322265625000000694, 0.05371093750000000694, 0.05419921875000000694, 0.05468750000000000694, 0.05517578125000000694, 0.05566406250000000694, 0.05615234375000000694, 0.05664062500000000694, 0.05712890625000000694, 0.05761718750000000694, 0.05810546875000000694, 0.05859375000000000694, 0.05908203125000000694, 0.05957031250000000694, 0.06005859375000000694, 0.06054687500000000694, 0.06103515625000000694, 0.06152343750000000694, 0.06201171875000000694, 0.06250000000000000000, 0.06298828125000000000, 0.06347656250000000000, 0.06396484375000000000, 0.06445312500000000000, 0.06494140625000000000, 0.06542968750000000000, 0.06591796875000000000, 0.06640625000000000000, 0.06689453125000000000, 0.06738281250000000000, 0.06787109375000000000, 0.06835937500000000000, 0.06884765625000000000, 0.06933593750000000000, 0.06982421875000000000, 0.07031250000000000000, 0.07080078125000000000, 0.07128906250000000000, 0.07177734375000000000, 0.07226562500000000000, 0.07275390625000000000, 0.07324218750000000000, 0.07373046875000000000, 0.07421875000000000000, 0.07470703125000000000, 0.07519531250000000000, 0.07568359375000000000, 0.07617187500000000000, 0.07666015625000000000, 0.07714843750000000000, 0.07763671875000000000, 0.07812500000000000000, 0.07861328125000000000, 0.07910156250000000000, 0.07958984375000000000, 0.08007812500000000000, 0.08056640625000000000, 0.08105468750000000000, 0.08154296875000000000, 0.08203125000000000000, 0.08251953125000000000, 0.08300781250000000000, 0.08349609375000000000, 0.08398437500000000000, 0.08447265625000000000, 0.08496093750000000000, 0.08544921875000000000, 0.08593750000000000000, 0.08642578125000000000, 0.08691406250000000000, 0.08740234375000000000, 0.08789062500000000000, 0.08837890625000000000, 0.08886718750000000000, 0.08935546875000000000, 0.08984375000000000000, 0.09033203125000000000, 0.09082031250000000000, 0.09130859375000000000, 0.09179687500000000000, 0.09228515625000000000, 0.09277343750000000000, 0.09326171875000000000, 0.09375000000000000000, 0.09423828125000001388, 0.09472656250000001388, 0.09521484375000001388, 0.09570312500000001388, 0.09619140625000001388, 0.09667968750000001388, 0.09716796875000001388, 0.09765625000000001388, 0.09814453125000001388, 0.09863281250000001388, 0.09912109375000001388, 0.09960937500000001388, 0.1000976562500000139, 0.1005859375000000139, 0.1010742187500000139, 0.1015625000000000139, 0.1020507812500000139, 0.1025390625000000139, 0.1030273437500000139, 0.1035156250000000139, 0.1040039062500000139, 0.1044921875000000139, 0.1049804687500000139, 0.1054687500000000139, 0.1059570312500000139, 0.1064453125000000139, 0.1069335937500000139, 0.1074218750000000139, 0.1079101562500000139, 0.1083984375000000139, 0.1088867187500000139, 0.1093750000000000139, 0.1098632812500000139, 0.1103515625000000139, 0.1108398437500000139, 0.1113281250000000139, 0.1118164062500000139, 0.1123046875000000139, 0.1127929687500000139, 0.1132812500000000139, 0.1137695312500000139, 0.1142578125000000139, 0.1147460937500000139, 0.1152343750000000139, 0.1157226562500000139, 0.1162109375000000139, 0.1166992187500000139, 0.1171875000000000139, 0.1176757812500000139, 0.1181640625000000139, 0.1186523437500000139, 0.1191406250000000139, 0.1196289062500000139, 0.1201171875000000139, 0.1206054687500000139, 0.1210937500000000139, 0.1215820312500000139, 0.1220703125000000139, 0.1225585937500000139, 0.1230468750000000139, 0.1235351562500000139, 0.1240234375000000139, 0.1245117187500000139, 0.1250000000000000000, 0.1254882812500000000, 0.1259765625000000000, 0.1264648437500000000, 0.1269531250000000000, 0.1274414062500000000, 0.1279296875000000000, 0.1284179687500000000, 0.1289062500000000000, 0.1293945312500000000, 0.1298828125000000000, 0.1303710937500000000, 0.1308593750000000000, 0.1313476562500000000, 0.1318359375000000000, 0.1323242187500000000, 0.1328125000000000000, 0.1333007812500000000, 0.1337890625000000000, 0.1342773437500000000, 0.1347656250000000000, 0.1352539062500000000, 0.1357421875000000000, 0.1362304687500000000, 0.1367187500000000000, 0.1372070312500000000, 0.1376953125000000000, 0.1381835937500000000, 0.1386718750000000000, 0.1391601562500000000, 0.1396484375000000000, 0.1401367187500000000, 0.1406250000000000000, 0.1411132812500000000, 0.1416015625000000000, 0.1420898437500000000, 0.1425781250000000000, 0.1430664062500000000, 0.1435546875000000000, 0.1440429687500000000, 0.1445312500000000000, 0.1450195312500000000, 0.1455078125000000000, 0.1459960937500000000, 0.1464843750000000000, 0.1469726562500000000, 0.1474609375000000000, 0.1479492187500000000, 0.1484375000000000000, 0.1489257812500000000, 0.1494140625000000000, 0.1499023437500000000, 0.1503906250000000000, 0.1508789062500000000, 0.1513671875000000000, 0.1518554687500000000, 0.1523437500000000000, 0.1528320312500000000, 0.1533203125000000000, 0.1538085937500000000, 0.1542968750000000000, 0.1547851562500000000, 0.1552734375000000000, 0.1557617187500000000, 0.1562500000000000000, 0.1567382812500000000, 0.1572265625000000000, 0.1577148437500000000, 0.1582031250000000000, 0.1586914062500000000, 0.1591796875000000000, 0.1596679687500000000, 0.1601562500000000000, 0.1606445312500000000, 0.1611328125000000000, 0.1616210937500000000, 0.1621093750000000000, 0.1625976562500000000, 0.1630859375000000000, 0.1635742187500000000, 0.1640625000000000000, 0.1645507812500000000, 0.1650390625000000000, 0.1655273437500000000, 0.1660156250000000000, 0.1665039062500000000, 0.1669921875000000000, 0.1674804687500000000, 0.1679687500000000000, 0.1684570312500000000, 0.1689453125000000000, 0.1694335937500000000, 0.1699218750000000000, 0.1704101562500000000, 0.1708984375000000000, 0.1713867187500000000, 0.1718750000000000000, 0.1723632812500000000, 0.1728515625000000000, 0.1733398437500000000, 0.1738281250000000000, 0.1743164062500000000, 0.1748046875000000000, 0.1752929687500000000, 0.1757812500000000000, 0.1762695312500000000, 0.1767578125000000000, 0.1772460937500000000, 0.1777343750000000000, 0.1782226562500000000, 0.1787109375000000000, 0.1791992187500000000, 0.1796875000000000000, 0.1801757812500000000, 0.1806640625000000000, 0.1811523437500000000, 0.1816406250000000000, 0.1821289062500000000, 0.1826171875000000000, 0.1831054687500000000, 0.1835937500000000000, 0.1840820312500000000, 0.1845703125000000000, 0.1850585937500000000, 0.1855468750000000000, 0.1860351562500000000, 0.1865234375000000000, 0.1870117187500000000, 0.1875000000000000000, 0.1879882812500000278, 0.1884765625000000278, 0.1889648437500000278, 0.1894531250000000278, 0.1899414062500000278, 0.1904296875000000278, 0.1909179687500000278, 0.1914062500000000278, 0.1918945312500000278, 0.1923828125000000278, 0.1928710937500000278, 0.1933593750000000278, 0.1938476562500000278, 0.1943359375000000278, 0.1948242187500000278, 0.1953125000000000278, 0.1958007812500000278, 0.1962890625000000278, 0.1967773437500000278, 0.1972656250000000278, 0.1977539062500000278, 0.1982421875000000278, 0.1987304687500000278, 0.1992187500000000278, 0.1997070312500000278, 0.2001953125000000278, 0.2006835937500000278, 0.2011718750000000278, 0.2016601562500000278, 0.2021484375000000278, 0.2026367187500000278, 0.2031250000000000278, 0.2036132812500000278, 0.2041015625000000278, 0.2045898437500000278, 0.2050781250000000278, 0.2055664062500000278, 0.2060546875000000278, 0.2065429687500000278, 0.2070312500000000278, 0.2075195312500000278, 0.2080078125000000278, 0.2084960937500000278, 0.2089843750000000278, 0.2094726562500000278, 0.2099609375000000278, 0.2104492187500000278, 0.2109375000000000278, 0.2114257812500000278, 0.2119140625000000278, 0.2124023437500000278, 0.2128906250000000278, 0.2133789062500000278, 0.2138671875000000278, 0.2143554687500000278, 0.2148437500000000278, 0.2153320312500000278, 0.2158203125000000278, 0.2163085937500000278, 0.2167968750000000278, 0.2172851562500000278, 0.2177734375000000278, 0.2182617187500000278, 0.2187500000000000278, 0.2192382812500000278, 0.2197265625000000278, 0.2202148437500000278, 0.2207031250000000278, 0.2211914062500000278, 0.2216796875000000278, 0.2221679687500000278, 0.2226562500000000278, 0.2231445312500000278, 0.2236328125000000278, 0.2241210937500000278, 0.2246093750000000278, 0.2250976562500000278, 0.2255859375000000278, 0.2260742187500000278, 0.2265625000000000278, 0.2270507812500000278, 0.2275390625000000278, 0.2280273437500000278, 0.2285156250000000278, 0.2290039062500000278, 0.2294921875000000278, 0.2299804687500000278, 0.2304687500000000278, 0.2309570312500000278, 0.2314453125000000278, 0.2319335937500000278, 0.2324218750000000278, 0.2329101562500000278, 0.2333984375000000278, 0.2338867187500000278, 0.2343750000000000278, 0.2348632812500000278, 0.2353515625000000278, 0.2358398437500000278, 0.2363281250000000278, 0.2368164062500000278, 0.2373046875000000278, 0.2377929687500000278, 0.2382812500000000278, 0.2387695312500000278, 0.2392578125000000278, 0.2397460937500000278, 0.2402343750000000278, 0.2407226562500000278, 0.2412109375000000278, 0.2416992187500000278, 0.2421875000000000278, 0.2426757812500000278, 0.2431640625000000278, 0.2436523437500000278, 0.2441406250000000278, 0.2446289062500000278, 0.2451171875000000278, 0.2456054687500000278, 0.2460937500000000278, 0.2465820312500000278, 0.2470703125000000278, 0.2475585937500000278, 0.2480468750000000278, 0.2485351562500000278, 0.2490234375000000278, 0.2495117187500000278, 0.2500000000000000000, 0.2504882812500000000, 0.2509765625000000000, 0.2514648437500000000, 0.2519531250000000000, 0.2524414062500000000, 0.2529296875000000000, 0.2534179687500000000, 0.2539062500000000000, 0.2543945312500000000, 0.2548828125000000000, 0.2553710937500000000, 0.2558593750000000000, 0.2563476562500000000, 0.2568359375000000000, 0.2573242187500000000, 0.2578125000000000000, 0.2583007812500000000, 0.2587890625000000000, 0.2592773437500000000, 0.2597656250000000000, 0.2602539062500000000, 0.2607421875000000000, 0.2612304687500000000, 0.2617187500000000000, 0.2622070312500000000, 0.2626953125000000000, 0.2631835937500000000, 0.2636718750000000000, 0.2641601562500000000, 0.2646484375000000000, 0.2651367187500000000, 0.2656250000000000000, 0.2661132812500000000, 0.2666015625000000000, 0.2670898437500000000, 0.2675781250000000000, 0.2680664062500000000, 0.2685546875000000000, 0.2690429687500000000, 0.2695312500000000000, 0.2700195312500000000, 0.2705078125000000000, 0.2709960937500000000, 0.2714843750000000000, 0.2719726562500000000, 0.2724609375000000000, 0.2729492187500000000, 0.2734375000000000000, 0.2739257812500000000, 0.2744140625000000000, 0.2749023437500000000, 0.2753906250000000000, 0.2758789062500000000, 0.2763671875000000000, 0.2768554687500000000, 0.2773437500000000000, 0.2778320312500000000, 0.2783203125000000000, 0.2788085937500000000, 0.2792968750000000000, 0.2797851562500000000, 0.2802734375000000000, 0.2807617187500000000, 0.2812500000000000000, 0.2817382812500000000, 0.2822265625000000000, 0.2827148437500000000, 0.2832031250000000000, 0.2836914062500000000, 0.2841796875000000000, 0.2846679687500000000, 0.2851562500000000000, 0.2856445312500000000, 0.2861328125000000000, 0.2866210937500000000, 0.2871093750000000000, 0.2875976562500000000, 0.2880859375000000000, 0.2885742187500000000, 0.2890625000000000000, 0.2895507812500000000, 0.2900390625000000000, 0.2905273437500000000, 0.2910156250000000000, 0.2915039062500000000, 0.2919921875000000000, 0.2924804687500000000, 0.2929687500000000000, 0.2934570312500000000, 0.2939453125000000000, 0.2944335937500000000, 0.2949218750000000000, 0.2954101562500000000, 0.2958984375000000000, 0.2963867187500000000, 0.2968750000000000000, 0.2973632812500000000, 0.2978515625000000000, 0.2983398437500000000, 0.2988281250000000000, 0.2993164062500000000, 0.2998046875000000000, 0.3002929687500000000, 0.3007812500000000000, 0.3012695312500000000, 0.3017578125000000000, 0.3022460937500000000, 0.3027343750000000000, 0.3032226562500000000, 0.3037109375000000000, 0.3041992187500000000, 0.3046875000000000000, 0.3051757812500000000, 0.3056640625000000000, 0.3061523437500000000, 0.3066406250000000000, 0.3071289062500000000, 0.3076171875000000000, 0.3081054687500000000, 0.3085937500000000000, 0.3090820312500000000, 0.3095703125000000000, 0.3100585937500000000, 0.3105468750000000000, 0.3110351562500000000, 0.3115234375000000000, 0.3120117187500000000, 0.3125000000000000000, 0.3129882812500000000, 0.3134765625000000000, 0.3139648437500000000, 0.3144531250000000000, 0.3149414062500000000, 0.3154296875000000000, 0.3159179687500000000, 0.3164062500000000000, 0.3168945312500000000, 0.3173828125000000000, 0.3178710937500000000, 0.3183593750000000000, 0.3188476562500000000, 0.3193359375000000000, 0.3198242187500000000, 0.3203125000000000000, 0.3208007812500000000, 0.3212890625000000000, 0.3217773437500000000, 0.3222656250000000000, 0.3227539062500000000, 0.3232421875000000000, 0.3237304687500000000, 0.3242187500000000000, 0.3247070312500000000, 0.3251953125000000000, 0.3256835937500000000, 0.3261718750000000000, 0.3266601562500000000, 0.3271484375000000000, 0.3276367187500000000, 0.3281250000000000000, 0.3286132812500000000, 0.3291015625000000000, 0.3295898437500000000, 0.3300781250000000000, 0.3305664062500000000, 0.3310546875000000000, 0.3315429687500000000, 0.3320312500000000000, 0.3325195312500000000, 0.3330078125000000000, 0.3334960937500000000, 0.3339843750000000000, 0.3344726562500000000, 0.3349609375000000000, 0.3354492187500000000, 0.3359375000000000000, 0.3364257812500000000, 0.3369140625000000000, 0.3374023437500000000, 0.3378906250000000000, 0.3383789062500000000, 0.3388671875000000000, 0.3393554687500000000, 0.3398437500000000000, 0.3403320312500000000, 0.3408203125000000000, 0.3413085937500000000, 0.3417968750000000000, 0.3422851562500000000, 0.3427734375000000000, 0.3432617187500000000, 0.3437500000000000000, 0.3442382812500000000, 0.3447265625000000000, 0.3452148437500000000, 0.3457031250000000000, 0.3461914062500000000, 0.3466796875000000000, 0.3471679687500000000, 0.3476562500000000000, 0.3481445312500000000, 0.3486328125000000000, 0.3491210937500000000, 0.3496093750000000000, 0.3500976562500000000, 0.3505859375000000000, 0.3510742187500000000, 0.3515625000000000000, 0.3520507812500000000, 0.3525390625000000000, 0.3530273437500000000, 0.3535156250000000000, 0.3540039062500000000, 0.3544921875000000000, 0.3549804687500000000, 0.3554687500000000000, 0.3559570312500000000, 0.3564453125000000000, 0.3569335937500000000, 0.3574218750000000000, 0.3579101562500000000, 0.3583984375000000000, 0.3588867187500000000, 0.3593750000000000000, 0.3598632812500000000, 0.3603515625000000000, 0.3608398437500000000, 0.3613281250000000000, 0.3618164062500000000, 0.3623046875000000000, 0.3627929687500000000, 0.3632812500000000000, 0.3637695312500000000, 0.3642578125000000000, 0.3647460937500000000, 0.3652343750000000000, 0.3657226562500000000, 0.3662109375000000000, 0.3666992187500000000, 0.3671875000000000000, 0.3676757812500000000, 0.3681640625000000000, 0.3686523437500000000, 0.3691406250000000000, 0.3696289062500000000, 0.3701171875000000000, 0.3706054687500000000, 0.3710937500000000000, 0.3715820312500000000, 0.3720703125000000000, 0.3725585937500000000, 0.3730468750000000000, 0.3735351562500000000, 0.3740234375000000000, 0.3745117187500000000, 0.3750000000000000000, 0.3754882812500000555, 0.3759765625000000555, 0.3764648437500000555, 0.3769531250000000555, 0.3774414062500000555, 0.3779296875000000555, 0.3784179687500000555, 0.3789062500000000555, 0.3793945312500000555, 0.3798828125000000555, 0.3803710937500000555, 0.3808593750000000555, 0.3813476562500000555, 0.3818359375000000555, 0.3823242187500000555, 0.3828125000000000555, 0.3833007812500000555, 0.3837890625000000555, 0.3842773437500000555, 0.3847656250000000555, 0.3852539062500000555, 0.3857421875000000555, 0.3862304687500000555, 0.3867187500000000555, 0.3872070312500000555, 0.3876953125000000555, 0.3881835937500000555, 0.3886718750000000555, 0.3891601562500000555, 0.3896484375000000555, 0.3901367187500000555, 0.3906250000000000555, 0.3911132812500000555, 0.3916015625000000555, 0.3920898437500000555, 0.3925781250000000555, 0.3930664062500000555, 0.3935546875000000555, 0.3940429687500000555, 0.3945312500000000555, 0.3950195312500000555, 0.3955078125000000555, 0.3959960937500000555, 0.3964843750000000555, 0.3969726562500000555, 0.3974609375000000555, 0.3979492187500000555, 0.3984375000000000555, 0.3989257812500000555, 0.3994140625000000555, 0.3999023437500000555, 0.4003906250000000555, 0.4008789062500000555, 0.4013671875000000555, 0.4018554687500000555, 0.4023437500000000555, 0.4028320312500000555, 0.4033203125000000555, 0.4038085937500000555, 0.4042968750000000555, 0.4047851562500000555, 0.4052734375000000555, 0.4057617187500000555, 0.4062500000000000555, 0.4067382812500000555, 0.4072265625000000555, 0.4077148437500000555, 0.4082031250000000555, 0.4086914062500000555, 0.4091796875000000555, 0.4096679687500000555, 0.4101562500000000555, 0.4106445312500000555, 0.4111328125000000555, 0.4116210937500000555, 0.4121093750000000555, 0.4125976562500000555, 0.4130859375000000555, 0.4135742187500000555, 0.4140625000000000555, 0.4145507812500000555, 0.4150390625000000555, 0.4155273437500000555, 0.4160156250000000555, 0.4165039062500000555, 0.4169921875000000555, 0.4174804687500000555, 0.4179687500000000555, 0.4184570312500000555, 0.4189453125000000555, 0.4194335937500000555, 0.4199218750000000555, 0.4204101562500000555, 0.4208984375000000555, 0.4213867187500000555, 0.4218750000000000555, 0.4223632812500000555, 0.4228515625000000555, 0.4233398437500000555, 0.4238281250000000555, 0.4243164062500000555, 0.4248046875000000555, 0.4252929687500000555, 0.4257812500000000555, 0.4262695312500000555, 0.4267578125000000555, 0.4272460937500000555, 0.4277343750000000555, 0.4282226562500000555, 0.4287109375000000555, 0.4291992187500000555, 0.4296875000000000555, 0.4301757812500000555, 0.4306640625000000555, 0.4311523437500000555, 0.4316406250000000555, 0.4321289062500000555, 0.4326171875000000555, 0.4331054687500000555, 0.4335937500000000555, 0.4340820312500000555, 0.4345703125000000555, 0.4350585937500000555, 0.4355468750000000555, 0.4360351562500000555, 0.4365234375000000555, 0.4370117187500000555, 0.4375000000000000555, 0.4379882812500000555, 0.4384765625000000555, 0.4389648437500000555, 0.4394531250000000555, 0.4399414062500000555, 0.4404296875000000555, 0.4409179687500000555, 0.4414062500000000555, 0.4418945312500000555, 0.4423828125000000555, 0.4428710937500000555, 0.4433593750000000555, 0.4438476562500000555, 0.4443359375000000555, 0.4448242187500000555, 0.4453125000000000555, 0.4458007812500000555, 0.4462890625000000555, 0.4467773437500000555, 0.4472656250000000555, 0.4477539062500000555, 0.4482421875000000555, 0.4487304687500000555, 0.4492187500000000555, 0.4497070312500000555, 0.4501953125000000555, 0.4506835937500000555, 0.4511718750000000555, 0.4516601562500000555, 0.4521484375000000555, 0.4526367187500000555, 0.4531250000000000555, 0.4536132812500000555, 0.4541015625000000555, 0.4545898437500000555, 0.4550781250000000555, 0.4555664062500000555, 0.4560546875000000555, 0.4565429687500000555, 0.4570312500000000555, 0.4575195312500000555, 0.4580078125000000555, 0.4584960937500000555, 0.4589843750000000555, 0.4594726562500000555, 0.4599609375000000555, 0.4604492187500000555, 0.4609375000000000555, 0.4614257812500000555, 0.4619140625000000555, 0.4624023437500000555, 0.4628906250000000555, 0.4633789062500000555, 0.4638671875000000555, 0.4643554687500000555, 0.4648437500000000555, 0.4653320312500000555, 0.4658203125000000555, 0.4663085937500000555, 0.4667968750000000555, 0.4672851562500000555, 0.4677734375000000555, 0.4682617187500000555, 0.4687500000000000555, 0.4692382812500000555, 0.4697265625000000555, 0.4702148437500000555, 0.4707031250000000555, 0.4711914062500000555, 0.4716796875000000555, 0.4721679687500000555, 0.4726562500000000555, 0.4731445312500000555, 0.4736328125000000555, 0.4741210937500000555, 0.4746093750000000555, 0.4750976562500000555, 0.4755859375000000555, 0.4760742187500000555, 0.4765625000000000555, 0.4770507812500000555, 0.4775390625000000555, 0.4780273437500000555, 0.4785156250000000555, 0.4790039062500000555, 0.4794921875000000555, 0.4799804687500000555, 0.4804687500000000555, 0.4809570312500000555, 0.4814453125000000555, 0.4819335937500000555, 0.4824218750000000555, 0.4829101562500000555, 0.4833984375000000555, 0.4838867187500000555, 0.4843750000000000555, 0.4848632812500000555, 0.4853515625000000555, 0.4858398437500000555, 0.4863281250000000555, 0.4868164062500000555, 0.4873046875000000555, 0.4877929687500000555, 0.4882812500000000555, 0.4887695312500000555, 0.4892578125000000555, 0.4897460937500000555, 0.4902343750000000555, 0.4907226562500000555, 0.4912109375000000555, 0.4916992187500000555, 0.4921875000000000555, 0.4926757812500000555, 0.4931640625000000555, 0.4936523437500000555, 0.4941406250000000555, 0.4946289062500000555, 0.4951171875000000555, 0.4956054687500000555, 0.4960937500000000555, 0.4965820312500000555, 0.4970703125000000555, 0.4975585937500000555, 0.4980468750000000555, 0.4985351562500000555, 0.4990234375000000555, 0.4995117187500000555, 0.5000000000000000000, 0.5004882812500000000, 0.5009765625000000000, 0.5014648437500000000, 0.5019531250000000000, 0.5024414062500000000, 0.5029296875000000000, 0.5034179687500000000, 0.5039062500000000000, 0.5043945312500000000, 0.5048828125000000000, 0.5053710937500000000, 0.5058593750000000000, 0.5063476562500000000, 0.5068359375000000000, 0.5073242187500000000, 0.5078125000000000000, 0.5083007812500000000, 0.5087890625000000000, 0.5092773437500000000, 0.5097656250000000000, 0.5102539062500000000, 0.5107421875000000000, 0.5112304687500000000, 0.5117187500000000000, 0.5122070312500000000, 0.5126953125000000000, 0.5131835937500000000, 0.5136718750000000000, 0.5141601562500000000, 0.5146484375000000000, 0.5151367187500000000, 0.5156250000000000000, 0.5161132812500000000, 0.5166015625000000000, 0.5170898437500000000, 0.5175781250000000000, 0.5180664062500000000, 0.5185546875000000000, 0.5190429687500000000, 0.5195312500000000000, 0.5200195312500000000, 0.5205078125000000000, 0.5209960937500000000, 0.5214843750000000000, 0.5219726562500000000, 0.5224609375000000000, 0.5229492187500000000, 0.5234375000000000000, 0.5239257812500000000, 0.5244140625000000000, 0.5249023437500000000, 0.5253906250000000000, 0.5258789062500000000, 0.5263671875000000000, 0.5268554687500000000, 0.5273437500000000000, 0.5278320312500000000, 0.5283203125000000000, 0.5288085937500000000, 0.5292968750000000000, 0.5297851562500000000, 0.5302734375000000000, 0.5307617187500000000, 0.5312500000000000000, 0.5317382812500000000, 0.5322265625000000000, 0.5327148437500000000, 0.5332031250000000000, 0.5336914062500000000, 0.5341796875000000000, 0.5346679687500000000, 0.5351562500000000000, 0.5356445312500000000, 0.5361328125000000000, 0.5366210937500000000, 0.5371093750000000000, 0.5375976562500000000, 0.5380859375000000000, 0.5385742187500000000, 0.5390625000000000000, 0.5395507812500000000, 0.5400390625000000000, 0.5405273437500000000, 0.5410156250000000000, 0.5415039062500000000, 0.5419921875000000000, 0.5424804687500000000, 0.5429687500000000000, 0.5434570312500000000, 0.5439453125000000000, 0.5444335937500000000, 0.5449218750000000000, 0.5454101562500000000, 0.5458984375000000000, 0.5463867187500000000, 0.5468750000000000000, 0.5473632812500000000, 0.5478515625000000000, 0.5483398437500000000, 0.5488281250000000000, 0.5493164062500000000, 0.5498046875000000000, 0.5502929687500000000, 0.5507812500000000000, 0.5512695312500000000, 0.5517578125000000000, 0.5522460937500000000, 0.5527343750000000000, 0.5532226562500000000, 0.5537109375000000000, 0.5541992187500000000, 0.5546875000000000000, 0.5551757812500000000, 0.5556640625000000000, 0.5561523437500000000, 0.5566406250000000000, 0.5571289062500000000, 0.5576171875000000000, 0.5581054687500000000, 0.5585937500000000000, 0.5590820312500000000, 0.5595703125000000000, 0.5600585937500000000, 0.5605468750000000000, 0.5610351562500000000, 0.5615234375000000000, 0.5620117187500000000, 0.5625000000000000000, 0.5629882812500000000, 0.5634765625000000000, 0.5639648437500000000, 0.5644531250000000000, 0.5649414062500000000, 0.5654296875000000000, 0.5659179687500000000, 0.5664062500000000000, 0.5668945312500000000, 0.5673828125000000000, 0.5678710937500000000, 0.5683593750000000000, 0.5688476562500000000, 0.5693359375000000000, 0.5698242187500000000, 0.5703125000000000000, 0.5708007812500000000, 0.5712890625000000000, 0.5717773437500000000, 0.5722656250000000000, 0.5727539062500000000, 0.5732421875000000000, 0.5737304687500000000, 0.5742187500000000000, 0.5747070312500000000, 0.5751953125000000000, 0.5756835937500000000, 0.5761718750000000000, 0.5766601562500000000, 0.5771484375000000000, 0.5776367187500000000, 0.5781250000000000000, 0.5786132812500000000, 0.5791015625000000000, 0.5795898437500000000, 0.5800781250000000000, 0.5805664062500000000, 0.5810546875000000000, 0.5815429687500000000, 0.5820312500000000000, 0.5825195312500000000, 0.5830078125000000000, 0.5834960937500000000, 0.5839843750000000000, 0.5844726562500000000, 0.5849609375000000000, 0.5854492187500000000, 0.5859375000000000000, 0.5864257812500000000, 0.5869140625000000000, 0.5874023437500000000, 0.5878906250000000000, 0.5883789062500000000, 0.5888671875000000000, 0.5893554687500000000, 0.5898437500000000000, 0.5903320312500000000, 0.5908203125000000000, 0.5913085937500000000, 0.5917968750000000000, 0.5922851562500000000, 0.5927734375000000000, 0.5932617187500000000, 0.5937500000000000000, 0.5942382812500000000, 0.5947265625000000000, 0.5952148437500000000, 0.5957031250000000000, 0.5961914062500000000, 0.5966796875000000000, 0.5971679687500000000, 0.5976562500000000000, 0.5981445312500000000, 0.5986328125000000000, 0.5991210937500000000, 0.5996093750000000000, 0.6000976562500000000, 0.6005859375000000000, 0.6010742187500000000, 0.6015625000000000000, 0.6020507812500000000, 0.6025390625000000000, 0.6030273437500000000, 0.6035156250000000000, 0.6040039062500000000, 0.6044921875000000000, 0.6049804687500000000, 0.6054687500000000000, 0.6059570312500000000, 0.6064453125000000000, 0.6069335937500000000, 0.6074218750000000000, 0.6079101562500000000, 0.6083984375000000000, 0.6088867187500000000, 0.6093750000000000000, 0.6098632812500000000, 0.6103515625000000000, 0.6108398437500000000, 0.6113281250000000000, 0.6118164062500000000, 0.6123046875000000000, 0.6127929687500000000, 0.6132812500000000000, 0.6137695312500000000, 0.6142578125000000000, 0.6147460937500000000, 0.6152343750000000000, 0.6157226562500000000, 0.6162109375000000000, 0.6166992187500000000, 0.6171875000000000000, 0.6176757812500000000, 0.6181640625000000000, 0.6186523437500000000, 0.6191406250000000000, 0.6196289062500000000, 0.6201171875000000000, 0.6206054687500000000, 0.6210937500000000000, 0.6215820312500000000, 0.6220703125000000000, 0.6225585937500000000, 0.6230468750000000000, 0.6235351562500000000, 0.6240234375000000000, 0.6245117187500000000, 0.6250000000000000000, 0.6254882812500000000, 0.6259765625000000000, 0.6264648437500000000, 0.6269531250000000000, 0.6274414062500000000, 0.6279296875000000000, 0.6284179687500000000, 0.6289062500000000000, 0.6293945312500000000, 0.6298828125000000000, 0.6303710937500000000, 0.6308593750000000000, 0.6313476562500000000, 0.6318359375000000000, 0.6323242187500000000, 0.6328125000000000000, 0.6333007812500000000, 0.6337890625000000000, 0.6342773437500000000, 0.6347656250000000000, 0.6352539062500000000, 0.6357421875000000000, 0.6362304687500000000, 0.6367187500000000000, 0.6372070312500000000, 0.6376953125000000000, 0.6381835937500000000, 0.6386718750000000000, 0.6391601562500000000, 0.6396484375000000000, 0.6401367187500000000, 0.6406250000000000000, 0.6411132812500000000, 0.6416015625000000000, 0.6420898437500000000, 0.6425781250000000000, 0.6430664062500000000, 0.6435546875000000000, 0.6440429687500000000, 0.6445312500000000000, 0.6450195312500000000, 0.6455078125000000000, 0.6459960937500000000, 0.6464843750000000000, 0.6469726562500000000, 0.6474609375000000000, 0.6479492187500000000, 0.6484375000000000000, 0.6489257812500000000, 0.6494140625000000000, 0.6499023437500000000, 0.6503906250000000000, 0.6508789062500000000, 0.6513671875000000000, 0.6518554687500000000, 0.6523437500000000000, 0.6528320312500000000, 0.6533203125000000000, 0.6538085937500000000, 0.6542968750000000000, 0.6547851562500000000, 0.6552734375000000000, 0.6557617187500000000, 0.6562500000000000000, 0.6567382812500000000, 0.6572265625000000000, 0.6577148437500000000, 0.6582031250000000000, 0.6586914062500000000, 0.6591796875000000000, 0.6596679687500000000, 0.6601562500000000000, 0.6606445312500000000, 0.6611328125000000000, 0.6616210937500000000, 0.6621093750000000000, 0.6625976562500000000, 0.6630859375000000000, 0.6635742187500000000, 0.6640625000000000000, 0.6645507812500000000, 0.6650390625000000000, 0.6655273437500000000, 0.6660156250000000000, 0.6665039062500000000, 0.6669921875000000000, 0.6674804687500000000, 0.6679687500000000000, 0.6684570312500000000, 0.6689453125000000000, 0.6694335937500000000, 0.6699218750000000000, 0.6704101562500000000, 0.6708984375000000000, 0.6713867187500000000, 0.6718750000000000000, 0.6723632812500000000, 0.6728515625000000000, 0.6733398437500000000, 0.6738281250000000000, 0.6743164062500000000, 0.6748046875000000000, 0.6752929687500000000, 0.6757812500000000000, 0.6762695312500000000, 0.6767578125000000000, 0.6772460937500000000, 0.6777343750000000000, 0.6782226562500000000, 0.6787109375000000000, 0.6791992187500000000, 0.6796875000000000000, 0.6801757812500000000, 0.6806640625000000000, 0.6811523437500000000, 0.6816406250000000000, 0.6821289062500000000, 0.6826171875000000000, 0.6831054687500000000, 0.6835937500000000000, 0.6840820312500000000, 0.6845703125000000000, 0.6850585937500000000, 0.6855468750000000000, 0.6860351562500000000, 0.6865234375000000000, 0.6870117187500000000, 0.6875000000000000000, 0.6879882812500000000, 0.6884765625000000000, 0.6889648437500000000, 0.6894531250000000000, 0.6899414062500000000, 0.6904296875000000000, 0.6909179687500000000, 0.6914062500000000000, 0.6918945312500000000, 0.6923828125000000000, 0.6928710937500000000, 0.6933593750000000000, 0.6938476562500000000, 0.6943359375000000000, 0.6948242187500000000, 0.6953125000000000000, 0.6958007812500000000, 0.6962890625000000000, 0.6967773437500000000, 0.6972656250000000000, 0.6977539062500000000, 0.6982421875000000000, 0.6987304687500000000, 0.6992187500000000000, 0.6997070312500000000, 0.7001953125000000000, 0.7006835937500000000, 0.7011718750000000000, 0.7016601562500000000, 0.7021484375000000000, 0.7026367187500000000, 0.7031250000000000000, 0.7036132812500000000, 0.7041015625000000000, 0.7045898437500000000, 0.7050781250000000000, 0.7055664062500000000, 0.7060546875000000000, 0.7065429687500000000, 0.7070312500000000000, 0.7075195312500000000, 0.7080078125000000000, 0.7084960937500000000, 0.7089843750000000000, 0.7094726562500000000, 0.7099609375000000000, 0.7104492187500000000, 0.7109375000000000000, 0.7114257812500000000, 0.7119140625000000000, 0.7124023437500000000, 0.7128906250000000000, 0.7133789062500000000, 0.7138671875000000000, 0.7143554687500000000, 0.7148437500000000000, 0.7153320312500000000, 0.7158203125000000000, 0.7163085937500000000, 0.7167968750000000000, 0.7172851562500000000, 0.7177734375000000000, 0.7182617187500000000, 0.7187500000000000000, 0.7192382812500000000, 0.7197265625000000000, 0.7202148437500000000, 0.7207031250000000000, 0.7211914062500000000, 0.7216796875000000000, 0.7221679687500000000, 0.7226562500000000000, 0.7231445312500000000, 0.7236328125000000000, 0.7241210937500000000, 0.7246093750000000000, 0.7250976562500000000, 0.7255859375000000000, 0.7260742187500000000, 0.7265625000000000000, 0.7270507812500000000, 0.7275390625000000000, 0.7280273437500000000, 0.7285156250000000000, 0.7290039062500000000, 0.7294921875000000000, 0.7299804687500000000, 0.7304687500000000000, 0.7309570312500000000, 0.7314453125000000000, 0.7319335937500000000, 0.7324218750000000000, 0.7329101562500000000, 0.7333984375000000000, 0.7338867187500000000, 0.7343750000000000000, 0.7348632812500000000, 0.7353515625000000000, 0.7358398437500000000, 0.7363281250000000000, 0.7368164062500000000, 0.7373046875000000000, 0.7377929687500000000, 0.7382812500000000000, 0.7387695312500000000, 0.7392578125000000000, 0.7397460937500000000, 0.7402343750000000000, 0.7407226562500000000, 0.7412109375000000000, 0.7416992187500000000, 0.7421875000000000000, 0.7426757812500000000, 0.7431640625000000000, 0.7436523437500000000, 0.7441406250000000000, 0.7446289062500000000, 0.7451171875000000000, 0.7456054687500000000, 0.7460937500000000000, 0.7465820312500000000, 0.7470703125000000000, 0.7475585937500000000, 0.7480468750000000000, 0.7485351562500000000, 0.7490234375000000000, 0.7495117187500000000, 0.7500000000000000000, 0.7504882812500001110, 0.7509765625000001110, 0.7514648437500001110, 0.7519531250000001110, 0.7524414062500001110, 0.7529296875000001110, 0.7534179687500001110, 0.7539062500000001110, 0.7543945312500001110, 0.7548828125000001110, 0.7553710937500001110, 0.7558593750000001110, 0.7563476562500001110, 0.7568359375000001110, 0.7573242187500001110, 0.7578125000000001110, 0.7583007812500001110, 0.7587890625000001110, 0.7592773437500001110, 0.7597656250000001110, 0.7602539062500001110, 0.7607421875000001110, 0.7612304687500001110, 0.7617187500000001110, 0.7622070312500001110, 0.7626953125000001110, 0.7631835937500001110, 0.7636718750000001110, 0.7641601562500001110, 0.7646484375000001110, 0.7651367187500001110, 0.7656250000000001110, 0.7661132812500001110, 0.7666015625000001110, 0.7670898437500001110, 0.7675781250000001110, 0.7680664062500001110, 0.7685546875000001110, 0.7690429687500001110, 0.7695312500000001110, 0.7700195312500001110, 0.7705078125000001110, 0.7709960937500001110, 0.7714843750000001110, 0.7719726562500001110, 0.7724609375000001110, 0.7729492187500001110, 0.7734375000000001110, 0.7739257812500001110, 0.7744140625000001110, 0.7749023437500001110, 0.7753906250000001110, 0.7758789062500001110, 0.7763671875000001110, 0.7768554687500001110, 0.7773437500000001110, 0.7778320312500001110, 0.7783203125000001110, 0.7788085937500001110, 0.7792968750000001110, 0.7797851562500001110, 0.7802734375000001110, 0.7807617187500001110, 0.7812500000000001110, 0.7817382812500001110, 0.7822265625000001110, 0.7827148437500001110, 0.7832031250000001110, 0.7836914062500001110, 0.7841796875000001110, 0.7846679687500001110, 0.7851562500000001110, 0.7856445312500001110, 0.7861328125000001110, 0.7866210937500001110, 0.7871093750000001110, 0.7875976562500001110, 0.7880859375000001110, 0.7885742187500001110, 0.7890625000000001110, 0.7895507812500001110, 0.7900390625000001110, 0.7905273437500001110, 0.7910156250000001110, 0.7915039062500001110, 0.7919921875000001110, 0.7924804687500001110, 0.7929687500000001110, 0.7934570312500001110, 0.7939453125000001110, 0.7944335937500001110, 0.7949218750000001110, 0.7954101562500001110, 0.7958984375000001110, 0.7963867187500001110, 0.7968750000000001110, 0.7973632812500001110, 0.7978515625000001110, 0.7983398437500001110, 0.7988281250000001110, 0.7993164062500001110, 0.7998046875000001110, 0.8002929687500001110, 0.8007812500000001110, 0.8012695312500001110, 0.8017578125000001110, 0.8022460937500001110, 0.8027343750000001110, 0.8032226562500001110, 0.8037109375000001110, 0.8041992187500001110, 0.8046875000000001110, 0.8051757812500001110, 0.8056640625000001110, 0.8061523437500001110, 0.8066406250000001110, 0.8071289062500001110, 0.8076171875000001110, 0.8081054687500001110, 0.8085937500000001110, 0.8090820312500001110, 0.8095703125000001110, 0.8100585937500001110, 0.8105468750000001110, 0.8110351562500001110, 0.8115234375000001110, 0.8120117187500001110, 0.8125000000000001110, 0.8129882812500001110, 0.8134765625000001110, 0.8139648437500001110, 0.8144531250000001110, 0.8149414062500001110, 0.8154296875000001110, 0.8159179687500001110, 0.8164062500000001110, 0.8168945312500001110, 0.8173828125000001110, 0.8178710937500001110, 0.8183593750000001110, 0.8188476562500001110, 0.8193359375000001110, 0.8198242187500001110, 0.8203125000000001110, 0.8208007812500001110, 0.8212890625000001110, 0.8217773437500001110, 0.8222656250000001110, 0.8227539062500001110, 0.8232421875000001110, 0.8237304687500001110, 0.8242187500000001110, 0.8247070312500001110, 0.8251953125000001110, 0.8256835937500001110, 0.8261718750000001110, 0.8266601562500001110, 0.8271484375000001110, 0.8276367187500001110, 0.8281250000000001110, 0.8286132812500001110, 0.8291015625000001110, 0.8295898437500001110, 0.8300781250000001110, 0.8305664062500001110, 0.8310546875000001110, 0.8315429687500001110, 0.8320312500000001110, 0.8325195312500001110, 0.8330078125000001110, 0.8334960937500001110, 0.8339843750000001110, 0.8344726562500001110, 0.8349609375000001110, 0.8354492187500001110, 0.8359375000000001110, 0.8364257812500001110, 0.8369140625000001110, 0.8374023437500001110, 0.8378906250000001110, 0.8383789062500001110, 0.8388671875000001110, 0.8393554687500001110, 0.8398437500000001110, 0.8403320312500001110, 0.8408203125000001110, 0.8413085937500001110, 0.8417968750000001110, 0.8422851562500001110, 0.8427734375000001110, 0.8432617187500001110, 0.8437500000000001110, 0.8442382812500001110, 0.8447265625000001110, 0.8452148437500001110, 0.8457031250000001110, 0.8461914062500001110, 0.8466796875000001110, 0.8471679687500001110, 0.8476562500000001110, 0.8481445312500001110, 0.8486328125000001110, 0.8491210937500001110, 0.8496093750000001110, 0.8500976562500001110, 0.8505859375000001110, 0.8510742187500001110, 0.8515625000000001110, 0.8520507812500001110, 0.8525390625000001110, 0.8530273437500001110, 0.8535156250000001110, 0.8540039062500001110, 0.8544921875000001110, 0.8549804687500001110, 0.8554687500000001110, 0.8559570312500001110, 0.8564453125000001110, 0.8569335937500001110, 0.8574218750000001110, 0.8579101562500001110, 0.8583984375000001110, 0.8588867187500001110, 0.8593750000000001110, 0.8598632812500001110, 0.8603515625000001110, 0.8608398437500001110, 0.8613281250000001110, 0.8618164062500001110, 0.8623046875000001110, 0.8627929687500001110, 0.8632812500000001110, 0.8637695312500001110, 0.8642578125000001110, 0.8647460937500001110, 0.8652343750000001110, 0.8657226562500001110, 0.8662109375000001110, 0.8666992187500001110, 0.8671875000000001110, 0.8676757812500001110, 0.8681640625000001110, 0.8686523437500001110, 0.8691406250000001110, 0.8696289062500001110, 0.8701171875000001110, 0.8706054687500001110, 0.8710937500000001110, 0.8715820312500001110, 0.8720703125000001110, 0.8725585937500001110, 0.8730468750000001110, 0.8735351562500001110, 0.8740234375000001110, 0.8745117187500001110, 0.8750000000000001110, 0.8754882812500001110, 0.8759765625000001110, 0.8764648437500001110, 0.8769531250000001110, 0.8774414062500001110, 0.8779296875000001110, 0.8784179687500001110, 0.8789062500000001110, 0.8793945312500001110, 0.8798828125000001110, 0.8803710937500001110, 0.8808593750000001110, 0.8813476562500001110, 0.8818359375000001110, 0.8823242187500001110, 0.8828125000000001110, 0.8833007812500001110, 0.8837890625000001110, 0.8842773437500001110, 0.8847656250000001110, 0.8852539062500001110, 0.8857421875000001110, 0.8862304687500001110, 0.8867187500000001110, 0.8872070312500001110, 0.8876953125000001110, 0.8881835937500001110, 0.8886718750000001110, 0.8891601562500001110, 0.8896484375000001110, 0.8901367187500001110, 0.8906250000000001110, 0.8911132812500001110, 0.8916015625000001110, 0.8920898437500001110, 0.8925781250000001110, 0.8930664062500001110, 0.8935546875000001110, 0.8940429687500001110, 0.8945312500000001110, 0.8950195312500001110, 0.8955078125000001110, 0.8959960937500001110, 0.8964843750000001110, 0.8969726562500001110, 0.8974609375000001110, 0.8979492187500001110, 0.8984375000000001110, 0.8989257812500001110, 0.8994140625000001110, 0.8999023437500001110, 0.9003906250000001110, 0.9008789062500001110, 0.9013671875000001110, 0.9018554687500001110, 0.9023437500000001110, 0.9028320312500001110, 0.9033203125000001110, 0.9038085937500001110, 0.9042968750000001110, 0.9047851562500001110, 0.9052734375000001110, 0.9057617187500001110, 0.9062500000000001110, 0.9067382812500001110, 0.9072265625000001110, 0.9077148437500001110, 0.9082031250000001110, 0.9086914062500001110, 0.9091796875000001110, 0.9096679687500001110, 0.9101562500000001110, 0.9106445312500001110, 0.9111328125000001110, 0.9116210937500001110, 0.9121093750000001110, 0.9125976562500001110, 0.9130859375000001110, 0.9135742187500001110, 0.9140625000000001110, 0.9145507812500001110, 0.9150390625000001110, 0.9155273437500001110, 0.9160156250000001110, 0.9165039062500001110, 0.9169921875000001110, 0.9174804687500001110, 0.9179687500000001110, 0.9184570312500001110, 0.9189453125000001110, 0.9194335937500001110, 0.9199218750000001110, 0.9204101562500001110, 0.9208984375000001110, 0.9213867187500001110, 0.9218750000000001110, 0.9223632812500001110, 0.9228515625000001110, 0.9233398437500001110, 0.9238281250000001110, 0.9243164062500001110, 0.9248046875000001110, 0.9252929687500001110, 0.9257812500000001110, 0.9262695312500001110, 0.9267578125000001110, 0.9272460937500001110, 0.9277343750000001110, 0.9282226562500001110, 0.9287109375000001110, 0.9291992187500001110, 0.9296875000000001110, 0.9301757812500001110, 0.9306640625000001110, 0.9311523437500001110, 0.9316406250000001110, 0.9321289062500001110, 0.9326171875000001110, 0.9331054687500001110, 0.9335937500000001110, 0.9340820312500001110, 0.9345703125000001110, 0.9350585937500001110, 0.9355468750000001110, 0.9360351562500001110, 0.9365234375000001110, 0.9370117187500001110, 0.9375000000000001110, 0.9379882812500001110, 0.9384765625000001110, 0.9389648437500001110, 0.9394531250000001110, 0.9399414062500001110, 0.9404296875000001110, 0.9409179687500001110, 0.9414062500000001110, 0.9418945312500001110, 0.9423828125000001110, 0.9428710937500001110, 0.9433593750000001110, 0.9438476562500001110, 0.9443359375000001110, 0.9448242187500001110, 0.9453125000000001110, 0.9458007812500001110, 0.9462890625000001110, 0.9467773437500001110, 0.9472656250000001110, 0.9477539062500001110, 0.9482421875000001110, 0.9487304687500001110, 0.9492187500000001110, 0.9497070312500001110, 0.9501953125000001110, 0.9506835937500001110, 0.9511718750000001110, 0.9516601562500001110, 0.9521484375000001110, 0.9526367187500001110, 0.9531250000000001110, 0.9536132812500001110, 0.9541015625000001110, 0.9545898437500001110, 0.9550781250000001110, 0.9555664062500001110, 0.9560546875000001110, 0.9565429687500001110, 0.9570312500000001110, 0.9575195312500001110, 0.9580078125000001110, 0.9584960937500001110, 0.9589843750000001110, 0.9594726562500001110, 0.9599609375000001110, 0.9604492187500001110, 0.9609375000000001110, 0.9614257812500001110, 0.9619140625000001110, 0.9624023437500001110, 0.9628906250000001110, 0.9633789062500001110, 0.9638671875000001110, 0.9643554687500001110, 0.9648437500000001110, 0.9653320312500001110, 0.9658203125000001110, 0.9663085937500001110, 0.9667968750000001110, 0.9672851562500001110, 0.9677734375000001110, 0.9682617187500001110, 0.9687500000000001110, 0.9692382812500001110, 0.9697265625000001110, 0.9702148437500001110, 0.9707031250000001110, 0.9711914062500001110, 0.9716796875000001110, 0.9721679687500001110, 0.9726562500000001110, 0.9731445312500001110, 0.9736328125000001110, 0.9741210937500001110, 0.9746093750000001110, 0.9750976562500001110, 0.9755859375000001110, 0.9760742187500001110, 0.9765625000000001110, 0.9770507812500001110, 0.9775390625000001110, 0.9780273437500001110, 0.9785156250000001110, 0.9790039062500001110, 0.9794921875000001110, 0.9799804687500001110, 0.9804687500000001110, 0.9809570312500001110, 0.9814453125000001110, 0.9819335937500001110, 0.9824218750000001110, 0.9829101562500001110, 0.9833984375000001110, 0.9838867187500001110, 0.9843750000000001110, 0.9848632812500001110, 0.9853515625000001110, 0.9858398437500001110, 0.9863281250000001110, 0.9868164062500001110, 0.9873046875000001110, 0.9877929687500001110, 0.9882812500000001110, 0.9887695312500001110, 0.9892578125000001110, 0.9897460937500001110, 0.9902343750000001110, 0.9907226562500001110, 0.9912109375000001110, 0.9916992187500001110, 0.9921875000000001110, 0.9926757812500001110, 0.9931640625000001110, 0.9936523437500001110, 0.9941406250000001110, 0.9946289062500001110, 0.9951171875000001110, 0.9956054687500001110, 0.9960937500000001110, 0.9965820312500001110, 0.9970703125000001110, 0.9975585937500001110, 0.9980468750000001110, 0.9985351562500001110, 0.9990234375000001110, 0.9995117187500001110, 1.000000000000000000 ),
 .UNSPECIFIED. ) ;
#18992=CARTESIAN_POINT ( 'NONE',  ( 12.78316523911058944, -16.47895720935621711, 11.49999999999998934 ) ) ;
#18994=CARTESIAN_POINT ( 'NONE',  ( -40.34598903906039169, -25.11096149773888797, 2.835861264366675183 ) ) ;
#18997=CARTESIAN_POINT ( 'NONE',  ( -42.62287095715006302, -23.47596703998600276, 11.44779298504227505 ) ) ;
#18998=CARTESIAN_POINT ( 'NONE',  ( -11.11193726737652199, 17.91617163517716804, -1.500000000000002220 ) ) ;
#19002=CARTESIAN_POINT ( 'NONE',  ( -120.5523422370003885, -24.92592662359561473, 8.075495903018000021 ) ) ;
#19004=CARTESIAN_POINT ( 'NONE',  ( -96.62287095715005592, -23.48783264082478794, -1.443836473390061936 ) ) ;
#19006=CARTESIAN_POINT ( 'NONE',  ( -9.282276271697774916, -19.63344595494797673, -1.500000000000002220 ) ) ;
#19007=CARTESIAN_POINT ( 'NONE',  ( -79.80079360954597689, -25.07329833162646082, 7.418818858774966607 ) ) ;
#19008=CARTESIAN_POINT ( 'NONE',  ( 5.670930919660429836, -21.52877996283707418, 11.49999999999999645 ) ) ;
#19009=ORIENTED_EDGE ( 'NONE', *, *, #25512, .T. ) ;
#19010=CARTESIAN_POINT ( 'NONE',  ( -50.37830952628071657, -25.24728723542768805, 5.197789135022055085 ) ) ;
#19014=EDGE_LOOP ( 'NONE', ( #52625, #94894, #11886, #90636 ) ) ;
#19015=CARTESIAN_POINT ( 'NONE',  ( -40.62287095715004170, -24.15431212366387825, -0.2830839119429072182 ) ) ;
#19016=EDGE_LOOP ( 'NONE', ( #82754, #17350, #47335, #86015 ) ) ;
#19017=EDGE_CURVE ( 'NONE', #34994, #12406, #30130, .T. ) ;
#19019=CARTESIAN_POINT ( 'NONE',  ( -47.55620429048338593, -24.64965694238575011, 8.947790433994200043 ) ) ;
#19020=ADVANCED_FACE ( 'NONE', ( #53900 ), #46278, .F. ) ;
#19021=CARTESIAN_POINT ( 'NONE',  ( -121.5543303801803177, -24.34968618360933945, 0.1864209137778886083 ) ) ;
#19022=DIRECTION ( 'NONE',  ( -1.000000000000000000, -3.773278334444166432E-23, -8.201307841325785021E-29 ) ) ;
#19024=CARTESIAN_POINT ( 'NONE',  ( -105.5228709571500758, -24.92579138211019085, 1.929029949965658464 ) ) ;
#19026=CARTESIAN_POINT ( 'NONE',  ( -130.5728709571500588, -25.36495145570554399, 3.850034294483935859 ) ) ;
#19027=CARTESIAN_POINT ( 'NONE',  ( 19.77452139984142221, -10.64395493966388706, -1.500000000000002220 ) ) ;
#19028=VERTEX_POINT ( 'NONE', #45289 ) ;
#19029=CARTESIAN_POINT ( 'NONE',  ( -112.5204644665129479, -23.73791477778912551, 11.05961554403169878 ) ) ;
#19030=CARTESIAN_POINT ( 'NONE',  ( -101.5869878991651234, -24.51419770103158413, 9.386484678747175181 ) ) ;
#19033=LINE ( 'NONE', #64751, #61143 ) ;
#19034=CARTESIAN_POINT ( 'NONE',  ( -130.5728709571501156, -24.75152770810920444, 1.363349870542269526 ) ) ;
#19035=CARTESIAN_POINT ( 'NONE',  ( 19.52168601723349894, 1.684101417132040979, 11.49999999999998934 ) ) ;
#19036=B_SPLINE_SURFACE_WITH_KNOTS ( 'NONE', 3, 3, ( 
 ( #13876, #99106, #60582, #76759 ),
 ( #7259, #99598, #100089, #37228 ),
 ( #30603, #83890, #44847, #98614 ),
 ( #29106, #61575, #22969, #36729 ),
 ( #82397, #60082, #52457, #37719 ),
 ( #68678, #12875, #75771, #68180 ),
 ( #43849, #74778, #9263, #1166 ) ),
 .UNSPECIFIED., .F., .F., .F.,
 ( 4, 3, 4 ),
 ( 4, 4 ),
 ( 0.0004766839783827998963, 0.1029713700210901639, 0.2054660560637975308 ),
 ( 0.1295269466903908040, 0.1305994347416321311 ),
 .UNSPECIFIED. ) ;
#19039=CARTESIAN_POINT ( 'NONE',  ( -21.45671390985790694, -1.711987587955616119, -1.500000000000002220 ) ) ;
#19042=CARTESIAN_POINT ( 'NONE',  ( -80.76567584835706270, -25.31572652954127278, 4.998963527312024979 ) ) ;
#19043=CARTESIAN_POINT ( 'NONE',  ( -100.5190840336241820, -25.12077108248912438, 2.833913962057982960 ) ) ;
#19044=FACE_OUTER_BOUND ( 'NONE', #71948, .T. ) ;
#19045=CARTESIAN_POINT ( 'NONE',  ( -18.50152239663938403, 13.63810111590111163, -1.500000000000002220 ) ) ;
#19049=CARTESIAN_POINT ( 'NONE',  ( -101.5228709571500758, -29.50248528299804818, 1.056150453629042030 ) ) ;
#19050=CARTESIAN_POINT ( 'NONE',  ( 15.17442925503088169, 13.16703847180013831, 11.49999999999999645 ) ) ;
#19051=DIRECTION ( 'NONE',  ( -3.773278334453079030E-23, 0.9999999999976377785, 2.173523156925979128E-06 ) ) ;
#19053=CARTESIAN_POINT ( 'NONE',  ( -99.52287095715000476, -23.73907113217737574, -1.053371485780073558 ) ) ;
#19056=CARTESIAN_POINT ( 'NONE',  ( -15.96263503330635380, 11.84234753045382682, 11.49999999999998934 ) ) ;
#19057=CARTESIAN_POINT ( 'NONE',  ( -94.52287095715006160, -24.64965694238575011, 8.947790433994196491 ) ) ;
#19058=CARTESIAN_POINT ( 'NONE',  ( 3.912202881759007767, 19.34271161525698091, -1.500000000000002220 ) ) ;
#19062=CARTESIAN_POINT ( 'NONE',  ( -98.62287095715005592, -29.50248528299804818, 1.056150453629042030 ) ) ;
#19064=CARTESIAN_POINT ( 'NONE',  ( -4.704028875484805639, -20.06825252194306941, 11.49999999999999645 ) ) ;
#19067=B_SPLINE_CURVE_WITH_KNOTS ( 'NONE', 3,
 ( #78376, #9374, #71286, #1774, #87001, #71790, #32712, #56575, #63696, #17490, #48456, #41850, #72791, #65695, #42846, #34227, #3293, #26106 ),
 .UNSPECIFIED., .F., .F.,
 ( 4, 2, 2, 2, 2, 2, 2, 2, 4 ),
 ( 0.000000000000000000, 0.1249999999999993894, 0.1874999999999992506, 0.2499999999999991118, 0.4999999999999995559, 0.7500000000000001110, 0.8125000000000001110, 0.8750000000000001110, 1.000000000000000000 ),
 .UNSPECIFIED. ) ;
#19068=CARTESIAN_POINT ( 'NONE',  ( -6.316168294299441932, 21.79233575779346310, 11.49999999999999645 ) ) ;
#19069=ORIENTED_EDGE ( 'NONE', *, *, #82072, .T. ) ;
#19070=CARTESIAN_POINT ( 'NONE',  ( -115.6228709571500417, -25.00182538069145721, 7.747789668545097541 ) ) ;
#19071=CARTESIAN_POINT ( 'NONE',  ( -97.58474497804847658, -24.65952944569304961, 1.056160979905703456 ) ) ;
#19075=FACE_OUTER_BOUND ( 'NONE', #66737, .T. ) ;
#19076=ORIENTED_EDGE ( 'NONE', *, *, #61268, .F. ) ;
#19077=CARTESIAN_POINT ( 'NONE',  ( -100.1661903510885452, -25.12553550024694360, 7.087413643504399730 ) ) ;
#19078=CARTESIAN_POINT ( 'NONE',  ( -1.055347110731411187, -22.84297022578905612, -1.500000000000002220 ) ) ;
#19080=CARTESIAN_POINT ( 'NONE',  ( -113.6295968303889481, -23.73791477778912196, 11.05961554403170233 ) ) ;
#19081=CARTESIAN_POINT ( 'NONE',  ( -63.49149983805614283, -24.66019654487200086, 8.947790411086119278 ) ) ;
#19082=ADVANCED_FACE ( 'NONE', ( #47288 ), #78703, .T. ) ;
#19083=CARTESIAN_POINT ( 'NONE',  ( -6.794891441663577503, 21.43730618243864683, 11.49999999999999645 ) ) ;
#19086=CARTESIAN_POINT ( 'NONE',  ( -11.46427080702723522, -18.74017919159951973, 11.49999999999998934 ) ) ;
#19087=EDGE_CURVE ( 'NONE', #89410, #97387, #55687, .T. ) ;
#19088=CARTESIAN_POINT ( 'NONE',  ( -111.5539232054254484, -24.15543982623907482, -0.2315651400026575712 ) ) ;
#19089=CARTESIAN_POINT ( 'NONE',  ( -29.23483314410334444, -24.79699843522629976, 5.425067535242146022 ) ) ;
#19091=CARTESIAN_POINT ( 'NONE',  ( -63.62287095715004881, -23.72773821059535493, 11.05748984161097503 ) ) ;
#19092=CARTESIAN_POINT ( 'NONE',  ( -111.6228709571500559, -23.94994826722515668, -0.6494450866351696439 ) ) ;
#19093=ORIENTED_EDGE ( 'NONE', *, *, #26231, .T. ) ;
#19094=CARTESIAN_POINT ( 'NONE',  ( -77.62287095715005592, -23.94994826722515668, -0.6494450866351729745 ) ) ;
#19095=CARTESIAN_POINT ( 'NONE',  ( -10.27258457790969892, -17.75692283049141196, 11.49999999999998934 ) ) ;
#19096=EDGE_LOOP ( 'NONE', ( #17727, #35, #21318, #53269 ) ) ;
#19097=ORIENTED_EDGE ( 'NONE', *, *, #49282, .F. ) ;
#19098=EDGE_LOOP ( 'NONE', ( #26874, #39778, #73918 ) ) ;
#19100=CARTESIAN_POINT ( 'NONE',  ( -0.07435467474217070938, 23.09247799282200475, -1.500000000000002220 ) ) ;
#19101=CARTESIAN_POINT ( 'NONE',  ( -104.5173939172612734, -23.96169478059714208, 10.65365249895717525 ) ) ;
#19103=CARTESIAN_POINT ( 'NONE',  ( -13.67433444753018534, -15.09191755960682890, -1.500000000000002220 ) ) ;
#19107=CARTESIAN_POINT ( 'NONE',  ( -29.51207664681304976, -23.65098756497642540, 11.05961561336856391 ) ) ;
#19108=B_SPLINE_CURVE_WITH_KNOTS ( 'NONE', 3,
 ( #47896, #40773, #210, #33156, #17939, #3726 ),
 .UNSPECIFIED., .F., .F.,
 ( 4, 2, 4 ),
 ( 6.391158118961562613E-06, 0.001387004593080782460, 0.002767618028042603297 ),
 .UNSPECIFIED. ) ;
#19109=CARTESIAN_POINT ( 'NONE',  ( -105.6261443220027445, -24.73486907724918282, 1.287355809206962576 ) ) ;
#19110=CARTESIAN_POINT ( 'NONE',  ( -63.52287095715009002, -23.72773821059535848, 11.05748984161097503 ) ) ;
#19112=CARTESIAN_POINT ( 'NONE',  ( -29.23473450784903704, -24.76881327774048458, 4.453843528195366552 ) ) ;
#19113=CARTESIAN_POINT ( 'NONE',  ( -90.22287095715005023, -23.47593901973090524, -1.443836447538996870 ) ) ;
#19115=CARTESIAN_POINT ( 'NONE',  ( -18.78340662496949776, 8.880393494302802893, -1.500000000000002220 ) ) ;
#19117=CARTESIAN_POINT ( 'NONE',  ( -96.62287095715005592, -29.50250243563736774, 8.947779886222138046 ) ) ;
#19118=VERTEX_POINT ( 'NONE', #25441 ) ;
#19119=B_SPLINE_SURFACE_WITH_KNOTS ( 'NONE', 3, 1, ( 
 ( #25309, #64409 ),
 ( #72500, #81099 ),
 ( #2994, #11580 ),
 ( #33931, #32428 ),
 ( #9591, #40550 ),
 ( #71502, #1989 ),
 ( #25816, #56287 ),
 ( #79597, #56786 ),
 ( #90578, #14441 ),
 ( #6832, #29678 ),
 ( #54029, #15440 ),
 ( #100155, #23035 ),
 ( #37792, #21057 ),
 ( #69237, #30168 ),
 ( #46400, #67761 ),
 ( #36799, #52027 ),
 ( #76826, #91569 ),
 ( #30673, #60649 ),
 ( #28684, #14939 ) ),
 .UNSPECIFIED., .F., .F., .F.,
 ( 4, 1, 1, 1, 1, 1, 1, 1, 1, 1, 1, 1, 1, 1, 1, 1, 4 ),
 ( 2, 2 ),
 ( 0.000000000000000000, 0.05733942592015824763, 0.1130633316232408925, 0.1691814487493780716, 0.2257745596549409484, 0.2838263038920837977, 0.3434542790864910655, 0.4059069615102774420, 0.4713922597696830752, 0.5380028337126923077, 0.6030635561963488822, 0.6676018307634233873, 0.7322254428169042706, 0.7970048098289836958, 0.8630479900344357747, 0.9303569870570429501, 1.000000000000000000 ),
 ( 0.000000000000000000, 1.000000000000000000 ),
 .UNSPECIFIED. ) ;
#19121=CARTESIAN_POINT ( 'NONE',  ( -107.6228709571501412, -23.94994826722516379, -0.6494450866351700880 ) ) ;
#19123=EDGE_LOOP ( 'NONE', ( #4288, #10005, #48926, #23859 ) ) ;
#19125=CARTESIAN_POINT ( 'NONE',  ( -116.6228709571500417, -24.51387760970724017, 9.387446482453407626 ) ) ;
#19126=CARTESIAN_POINT ( 'NONE',  ( -74.62287095715004170, -23.94994826722566117, -0.6494450866342730277 ) ) ;
#19128=CARTESIAN_POINT ( 'NONE',  ( 2.303347834742990763, 21.97011321758780866, 11.49999999999999645 ) ) ;
#19130=CARTESIAN_POINT ( 'NONE',  ( -103.5574459519354065, -23.73766607897670156, -1.055555164236454901 ) ) ;
#19131=CARTESIAN_POINT ( 'NONE',  ( 6.494847429386178206, -21.66115869805930672, 11.49999999999998934 ) ) ;
#19132=AXIS2_PLACEMENT_3D ( 'NONE', #22641, #1339, #7934 ) ;
#19133=CARTESIAN_POINT ( 'NONE',  ( -115.5872429041571650, -24.92592662359561473, 8.075495903017996469 ) ) ;
#19134=ORIENTED_EDGE ( 'NONE', *, *, #86227, .T. ) ;
#19135=EDGE_CURVE ( 'NONE', #59566, #89278, #48296, .T. ) ;
#19136=EDGE_LOOP ( 'NONE', ( #28232, #27197, #61106, #64820 ) ) ;
#19138=EDGE_CURVE ( 'NONE', #12730, #24728, #1219, .T. ) ;
#19143=ORIENTED_EDGE ( 'NONE', *, *, #94033, .T. ) ;
#19144=CARTESIAN_POINT ( 'NONE',  ( 12.09327641706010326, 17.40255341615222306, 11.49999999999998934 ) ) ;
#19145=VECTOR ( 'NONE', #31207, 1000.000000000000114 ) ;
#19147=CARTESIAN_POINT ( 'NONE',  ( -80.62287095715008434, -24.83620972994592080, 8.398175272781369216 ) ) ;
#19148=CARTESIAN_POINT ( 'NONE',  ( -2.790049085472659396, -22.09070898310802633, -1.500000000000002220 ) ) ;
#19149=CARTESIAN_POINT ( 'NONE',  ( -49.87826110250815503, -25.03220892416941723, 7.497148264617506719 ) ) ;
#19150=ORIENTED_EDGE ( 'NONE', *, *, #12338, .F. ) ;
#19152=CARTESIAN_POINT ( 'NONE',  ( -48.58953762381671737, -24.65952944569304250, 1.056160979905691466 ) ) ;
#19153=DIRECTION ( 'NONE',  ( -3.773278334453079618E-23, 0.9999999999976377785, 2.173523156925979975E-06 ) ) ;
#19155=CARTESIAN_POINT ( 'NONE',  ( 6.966380261627926451, -18.21767524041069564, -1.500000000000002220 ) ) ;
#19156=CARTESIAN_POINT ( 'NONE',  ( 19.99082695160776169, -7.785253749782737209, 11.49999999999998934 ) ) ;
#19157=CARTESIAN_POINT ( 'NONE',  ( -26.15505896238250472, -24.57999669887485794, 2.424162796277344434 ) ) ;
#19158=DIRECTION ( 'NONE',  ( 0.000000000000000000, 2.173523156925980399E-06, -0.9999999999976378895 ) ) ;
#19159=CARTESIAN_POINT ( 'NONE',  ( -77.63799161339106547, -23.96119346886880663, -0.6495511937832126881 ) ) ;
#19160=CARTESIAN_POINT ( 'NONE',  ( 18.68554041145753786, -12.99315341008173519, -1.500000000000002220 ) ) ;
#19161=ADVANCED_FACE ( 'NONE', ( #8222 ), #1618, .T. ) ;
#19163=FACE_OUTER_BOUND ( 'NONE', #45316, .T. ) ;
#19165=CARTESIAN_POINT ( 'NONE',  ( -14.97016004668225264, 13.15154794113874637, 11.49999999999999645 ) ) ;
#19166=CARTESIAN_POINT ( 'NONE',  ( -104.5599225995679404, -23.48783264082477373, -1.443836473390085695 ) ) ;
#19169=FACE_OUTER_BOUND ( 'NONE', #3533, .T. ) ;
#19170=VERTEX_POINT ( 'NONE', #86344 ) ;
#19172=CARTESIAN_POINT ( 'NONE',  ( -32.42034289422212368, -24.87219037988794312, 1.747789950295619787 ) ) ;
#19173=CARTESIAN_POINT ( 'NONE',  ( 14.13103794885040898, -16.47871000921984219, -1.500000000000002220 ) ) ;
#19175=CARTESIAN_POINT ( 'NONE',  ( -56.50279899131798089, -24.15620529776628445, 10.23563542870660648 ) ) ;
#19176=CARTESIAN_POINT ( 'NONE',  ( -15.27948257512286645, 12.15582775940324822, -1.500000000000002220 ) ) ;
#19178=CARTESIAN_POINT ( 'NONE',  ( -55.49531503891194717, -24.40133493613049964, 9.663955038902800609 ) ) ;
#19179=B_SPLINE_CURVE_WITH_KNOTS ( 'NONE', 3,
 ( #97928, #81225, #26939, #88850 ),
 .UNSPECIFIED., .F., .F.,
 ( 4, 4 ),
 ( 0.2089094642748469122, 0.2099102113156124105 ),
 .UNSPECIFIED. ) ;
#19180=VERTEX_POINT ( 'NONE', #16324 ) ;
#19183=CARTESIAN_POINT ( 'NONE',  ( 16.50020720150075348, -12.08490501797973238, 11.49999999999999645 ) ) ;
#19184=DIRECTION ( 'NONE',  ( 3.773278334444167608E-23, -1.000000000000000000, 0.000000000000000000 ) ) ;
#19185=DIRECTION ( 'NONE',  ( 3.773278334444167608E-23, -1.000000000000000000, 0.000000000000000000 ) ) ;
#19186=ORIENTED_EDGE ( 'NONE', *, *, #99289, .F. ) ;
#19187=CARTESIAN_POINT ( 'NONE',  ( -55.55620429048339304, -23.48786465467241058, 11.44779295918254469 ) ) ;
#19188=CARTESIAN_POINT ( 'NONE',  ( -39.48699591144466581, -25.28892559316353683, 3.925286840877467487 ) ) ;
#19189=FACE_OUTER_BOUND ( 'NONE', #9148, .T. ) ;
#19191=EDGE_CURVE ( 'NONE', #44968, #60374, #27810, .T. ) ;
#19195=VECTOR ( 'NONE', #28047, 1000.000000000000114 ) ;
#19196=CARTESIAN_POINT ( 'NONE',  ( 3.160899137004691717, 22.77513019406404382, 11.49999999999999645 ) ) ;
#19197=CARTESIAN_POINT ( 'NONE',  ( 22.69831151501224298, -1.600861625767590724, 11.49999999999998934 ) ) ;
#19200=CARTESIAN_POINT ( 'NONE',  ( -81.52287095715009002, -23.72773821059537269, 11.05748984161097503 ) ) ;
#19201=CARTESIAN_POINT ( 'NONE',  ( -78.55620429048339304, -23.48786465467241058, 11.44779295918254469 ) ) ;
#19203=CARTESIAN_POINT ( 'NONE',  ( -15.17958814119055155, -15.74432251006154715, -1.500000000000002220 ) ) ;
#19205=CARTESIAN_POINT ( 'NONE',  ( -74.52287095715007581, -23.72747288104470087, -1.053458166803227014 ) ) ;
#19207=CARTESIAN_POINT ( 'NONE',  ( -55.52287095715005449, -24.99132157543083821, 2.256160258750667502 ) ) ;
#19212=CARTESIAN_POINT ( 'NONE',  ( -20.42006937447004233, 0.3101567295262241952, -1.500000000000002220 ) ) ;
#19215=ORIENTED_EDGE ( 'NONE', *, *, #63310, .F. ) ;
#19216=ORIENTED_EDGE ( 'NONE', *, *, #44188, .T. ) ;
#19217=CARTESIAN_POINT ( 'NONE',  ( 22.97298546869389568, 1.202750762487129199, -1.500000000000002220 ) ) ;
#19219=ADVANCED_FACE ( 'NONE', ( #34065 ), #26455, .F. ) ;
#19220=CARTESIAN_POINT ( 'NONE',  ( 9.409760114191467295, 17.86087837679851020, -1.500000000000002220 ) ) ;
#19221=EDGE_LOOP ( 'NONE', ( #88281, #98190, #46964, #96349 ) ) ;
#19224=EDGE_CURVE ( 'NONE', #47870, #53939, #43182, .T. ) ;
#19226=FACE_OUTER_BOUND ( 'NONE', #93246, .T. ) ;
#19227=CARTESIAN_POINT ( 'NONE',  ( -53.50201011555726893, -24.15620529776627734, 10.23563542870660825 ) ) ;
#19228=AXIS2_PLACEMENT_3D ( 'NONE', #29546, #6210, #28066 ) ;
#19229=CARTESIAN_POINT ( 'NONE',  ( 12.02608574658498597, -17.65016651952024063, 11.49999999999999645 ) ) ;
#19231=CARTESIAN_POINT ( 'NONE',  ( -78.62287095715005592, -23.47596703998600631, 11.44779298504227860 ) ) ;
#19233=CARTESIAN_POINT ( 'NONE',  ( 21.27325221474336914, 6.521069146585026566, -1.500000000000002220 ) ) ;
#19234=CARTESIAN_POINT ( 'NONE',  ( -20.55277978778089576, -2.218614319624547360, 11.49999999999998934 ) ) ;
#19240=CARTESIAN_POINT ( 'NONE',  ( -50.04601614386864838, -25.27517885246146534, 2.868514059739770250 ) ) ;
#19241=CARTESIAN_POINT ( 'NONE',  ( -19.94816486946033507, 6.322790147265108018, -1.500000000000002220 ) ) ;
#19242=CARTESIAN_POINT ( 'NONE',  ( -21.91604229967229500, -0.6759211909499470705, 11.49999999999999645 ) ) ;
#19243=PLANE ( 'NONE',  #67404 ) ;
#19244=CARTESIAN_POINT ( 'NONE',  ( -21.69688529672534827, 6.072505851105969299, 11.49999999999998934 ) ) ;
#19245=CARTESIAN_POINT ( 'NONE',  ( 5.463070048063013218, -20.23478146675526190, 11.49999999999998934 ) ) ;
#19246=CARTESIAN_POINT ( 'NONE',  ( -26.22762954581084571, -24.97067058367230175, 6.176716003714248338 ) ) ;
#19252=ORIENTED_EDGE ( 'NONE', *, *, #36833, .F. ) ;
#19253=CARTESIAN_POINT ( 'NONE',  ( -52.51446550490977927, -23.73766607897671577, -1.055555164236436472 ) ) ;
#19255=CARTESIAN_POINT ( 'NONE',  ( 17.49997855696484095, 12.48231381050728928, -1.500000000000002220 ) ) ;
#19256=ORIENTED_EDGE ( 'NONE', *, *, #8060, .T. ) ;
#19258=CARTESIAN_POINT ( 'NONE',  ( -6.733481718715807141, 19.98004043397084928, -1.500000000000002220 ) ) ;
#19259=CARTESIAN_POINT ( 'NONE',  ( -60.58953762381671027, -25.00182538069145011, 7.747789668545099317 ) ) ;
#19261=VECTOR ( 'NONE', #60355, 1000.000000000000114 ) ;
#19262=CARTESIAN_POINT ( 'NONE',  ( -87.62287095715004170, -24.65952944569304606, 1.056160979905700348 ) ) ;
#19263=CARTESIAN_POINT ( 'NONE',  ( -101.5168375974609063, -23.96119346886880663, -0.6495511937832049165 ) ) ;
#19264=CARTESIAN_POINT ( 'NONE',  ( -51.55620429048340014, -23.48786465467241058, 11.44779295918254647 ) ) ;
#19265=CARTESIAN_POINT ( 'NONE',  ( -13.14421341422731260, -17.72855101262432242, -1.500000000000002220 ) ) ;
#19267=CARTESIAN_POINT ( 'NONE',  ( -116.5222328135519518, -23.48783264082478439, -1.443836473390061936 ) ) ;
#19269=CARTESIAN_POINT ( 'NONE',  ( -41.56322468833811712, -25.31624637032491165, 5.062029375606173609 ) ) ;
#19271=CARTESIAN_POINT ( 'NONE',  ( -26.95684302982099467, -24.86038313398945476, 2.662461283694073089 ) ) ;
#19273=CARTESIAN_POINT ( 'NONE',  ( -63.52287095715010423, -24.34917612406836795, 0.1852690917426547679 ) ) ;
#19274=CARTESIAN_POINT ( 'NONE',  ( -5.188002292566340934, -20.72503599944539587, 11.49999999999998934 ) ) ;
#19275=CARTESIAN_POINT ( 'NONE',  ( -121.5562042904833504, -24.64965694238575367, 8.947790433994189385 ) ) ;
#19276=CARTESIAN_POINT ( 'NONE',  ( -91.16087763667918864, -25.31973986624387862, 5.294390042787146200 ) ) ;
#19277=CARTESIAN_POINT ( 'NONE',  ( -64.64730567560253860, -23.73791477778911840, 11.05961554403170766 ) ) ;
#19278=CARTESIAN_POINT ( 'NONE',  ( -80.72042306966947933, -25.12719728850807499, 7.077500010625388249 ) ) ;
#19279=CARTESIAN_POINT ( 'NONE',  ( 9.831018646898828095, -20.30805102056165623, -1.500000000000002220 ) ) ;
#19280=ADVANCED_FACE ( 'NONE', ( #20311 ), #88857, .T. ) ;
#19281=LINE ( 'NONE', #81192, #53922 ) ;
#19282=ORIENTED_EDGE ( 'NONE', *, *, #80310, .T. ) ;
#19284=CARTESIAN_POINT ( 'NONE',  ( -99.62287095715005592, -23.47593901973091235, -1.443836447539001089 ) ) ;
#19285=CARTESIAN_POINT ( 'NONE',  ( 6.816645498261984848, 18.52099371530728789, 11.49999999999999645 ) ) ;
#19286=CARTESIAN_POINT ( 'NONE',  ( -67.52287095715006160, -29.50248528299804818, 1.056150453629036701 ) ) ;
#19287=VECTOR ( 'NONE', #19947, 1000.000000000000114 ) ;
#19288=CARTESIAN_POINT ( 'NONE',  ( -119.5228709571500616, -23.48783264082477018, -1.443836473390082142 ) ) ;
#19289=ORIENTED_EDGE ( 'NONE', *, *, #65073, .T. ) ;
#19290=CARTESIAN_POINT ( 'NONE',  ( -42.58953762381671737, -23.47593901973091235, -1.443836447539011525 ) ) ;
#19291=CARTESIAN_POINT ( 'NONE',  ( -29.79725469281722994, -24.60094484029862372, 4.359878766298754371 ) ) ;
#19292=DIRECTION ( 'NONE',  ( 1.000000000000000000, 3.773278334444166432E-23, 8.201307841325785021E-29 ) ) ;
#19293=EDGE_CURVE ( 'NONE', #7634, #20357, #77392, .T. ) ;
#19294=CARTESIAN_POINT ( 'NONE',  ( -19.98381242416700587, 8.274006965216138099, 11.49999999999998934 ) ) ;
#19296=CARTESIAN_POINT ( 'NONE',  ( -126.6228709571500275, -23.95044443724993499, 10.65354141964649592 ) ) ;
#19297=CARTESIAN_POINT ( 'NONE',  ( -101.5228709571500758, -23.48786465467241769, 11.44779295918254114 ) ) ;
#19298=EDGE_CURVE ( 'NONE', #19368, #96700, #35565, .T. ) ;
#19299=CARTESIAN_POINT ( 'NONE',  ( -92.55620429048337883, -23.48783264082478084, -1.443836473390063269 ) ) ;
#19300=FACE_OUTER_BOUND ( 'NONE', #29863, .T. ) ;
#19301=CARTESIAN_POINT ( 'NONE',  ( 10.99584971316270732, 16.45119811332560289, -1.500000000000002220 ) ) ;
#19302=ORIENTED_EDGE ( 'NONE', *, *, #6831, .T. ) ;
#19304=CARTESIAN_POINT ( 'NONE',  ( 15.69265952521009488, -12.80212094623039576, 11.49999999999999645 ) ) ;
#19307=ORIENTED_EDGE ( 'NONE', *, *, #19791, .F. ) ;
#19309=DIRECTION ( 'NONE',  ( -3.773278334453079618E-23, 0.9999999999976377785, 2.173523156925979975E-06 ) ) ;
#19311=CARTESIAN_POINT ( 'NONE',  ( -103.6228709571500559, -23.72773821059535493, 11.05748984161097681 ) ) ;
#19313=CARTESIAN_POINT ( 'NONE',  ( 17.53424486177994623, -9.724335930198575895, 11.49999999999998934 ) ) ;
#19315=LINE ( 'NONE', #35057, #58063 ) ;
#19316=ORIENTED_EDGE ( 'NONE', *, *, #18778, .T. ) ;
#19317=B_SPLINE_CURVE_WITH_KNOTS ( 'NONE', 3,
 ( #52626, #90685, #53141, #21164 ),
 .UNSPECIFIED., .F., .F.,
 ( 4, 4 ),
 ( 0.2599715638078484714, 0.2689779950799639496 ),
 .UNSPECIFIED. ) ;
#19319=CARTESIAN_POINT ( 'NONE',  ( -73.62287095715005592, -24.64965695001468404, 8.947790433994184056 ) ) ;
#19320=CARTESIAN_POINT ( 'NONE',  ( -124.6228709571500559, -29.50250243563736774, 8.947779886222134493 ) ) ;
#19322=CARTESIAN_POINT ( 'NONE',  ( -105.5228709571500616, -23.84047902841601996, -0.8780736468305707643 ) ) ;
#19323=CARTESIAN_POINT ( 'NONE',  ( -73.51160046725669872, -23.96119346886880663, -0.6495511937832116889 ) ) ;
#19324=EDGE_CURVE ( 'NONE', #99120, #50584, #72634, .T. ) ;
#19325=CARTESIAN_POINT ( 'NONE',  ( -117.5228709571500758, -23.47596703998600631, 11.44779298504227860 ) ) ;
#19326=B_SPLINE_CURVE_WITH_KNOTS ( 'NONE', 3,
 ( #28283, #51631, #59750, #5940 ),
 .UNSPECIFIED., .F., .F.,
 ( 4, 4 ),
 ( 0.000000000000000000, 9.999999999998897304E-05 ),
 .UNSPECIFIED. ) ;
#19330=CARTESIAN_POINT ( 'NONE',  ( -13.46841296510753061, 15.22696965993213070, 11.49999999999998934 ) ) ;
#19332=B_SPLINE_CURVE_WITH_KNOTS ( 'NONE', 3,
 ( #59071, #28606, #42362, #80897 ),
 .UNSPECIFIED., .F., .F.,
 ( 4, 4 ),
 ( 0.8210863176411906661, 0.8300927489133060888 ),
 .UNSPECIFIED. ) ;
#19333=CARTESIAN_POINT ( 'NONE',  ( -2.941484630304247450, -22.72858670154147376, 11.49999999999998934 ) ) ;
#19334=EDGE_CURVE ( 'NONE', #39695, #69684, #67724, .T. ) ;
#19338=CARTESIAN_POINT ( 'NONE',  ( -49.12145562309674318, -25.27906036046082150, 4.198313730648785658 ) ) ;
#19340=CARTESIAN_POINT ( 'NONE',  ( -76.52287095715009002, -24.50216790748203977, 0.6166512839542565017 ) ) ;
#19342=CARTESIAN_POINT ( 'NONE',  ( -90.52287095715006160, -24.99156044556202616, 7.747789690856173195 ) ) ;
#19343=CARTESIAN_POINT ( 'NONE',  ( -21.21068194950259311, 0.7780057951688260642, 11.49999999999999645 ) ) ;
#19345=CARTESIAN_POINT ( 'NONE',  ( -22.11188964843745453, -1.696007508606716341, 11.49999999999998934 ) ) ;
#19346=CARTESIAN_POINT ( 'NONE',  ( 19.36870410414886479, 7.000668502413378569, -1.500000000000002220 ) ) ;
#19348=EDGE_LOOP ( 'NONE', ( #56717, #52952, #94623, #87388 ) ) ;
#19349=CARTESIAN_POINT ( 'NONE',  ( -41.64786393905067285, -23.96119346886880663, -0.6495511937831990323 ) ) ;
#19351=CARTESIAN_POINT ( 'NONE',  ( -54.65090589817863531, -23.73766607897669445, -1.055555164236461563 ) ) ;
#19352=CARTESIAN_POINT ( 'NONE',  ( -91.15361000704997707, -29.50249591506787894, 5.947779886229223045 ) ) ;
#19354=ORIENTED_EDGE ( 'NONE', *, *, #55210, .T. ) ;
#19355=B_SPLINE_CURVE_WITH_KNOTS ( 'NONE', 3,
 ( #66508, #34534, #88825, #26917 ),
 .UNSPECIFIED., .F., .F.,
 ( 4, 4 ),
 ( 0.000000000000000000, 1.000000000000000000 ),
 .UNSPECIFIED. ) ;
#19356=ORIENTED_EDGE ( 'NONE', *, *, #67881, .F. ) ;
#19358=CARTESIAN_POINT ( 'NONE',  ( -108.5895376238166961, -24.65952944569304961, 1.056160979905701014 ) ) ;
#19359=CARTESIAN_POINT ( 'NONE',  ( -130.5728709571500588, -23.53198925593397917, 11.48393099501408976 ) ) ;
#19360=CARTESIAN_POINT ( 'NONE',  ( 9.628234360240019996, 18.42577530400075858, -1.500000000000002220 ) ) ;
#19361=CARTESIAN_POINT ( 'NONE',  ( 16.02445091669267185, 14.69945503153335764, 11.49999999999999645 ) ) ;
#19365=CARTESIAN_POINT ( 'NONE',  ( 22.03792223356247604, -4.036589945906135846, 11.49999999999998934 ) ) ;
#19368=VERTEX_POINT ( 'NONE', #22804 ) ;
#19370=CARTESIAN_POINT ( 'NONE',  ( -85.62287095715004170, -24.99132157543083821, 2.256160258750667502 ) ) ;
#19371=B_SPLINE_CURVE_WITH_KNOTS ( 'NONE', 3,
 ( #33893, #47632, #87179, #9054, #25779, #40005, #79059, #63872 ),
 .UNSPECIFIED., .F., .F.,
 ( 4, 2, 2, 4 ),
 ( -0.001240355328176776396, -0.0002398155169398860729, 0.0007607242942970042499, 0.002761803916770786630 ),
 .UNSPECIFIED. ) ;
#19372=ORIENTED_EDGE ( 'NONE', *, *, #18311, .F. ) ;
#19374=DIRECTION ( 'NONE',  ( 0.000000000000000000, -2.173523156925979552E-06, 0.9999999999976378895 ) ) ;
#19376=CARTESIAN_POINT ( 'NONE',  ( -7.839647760473957838, 19.78794240023834661, -1.500000000000002220 ) ) ;
#19378=CARTESIAN_POINT ( 'NONE',  ( -88.55141844598099965, -24.15543982623907127, -0.2315651400026634277 ) ) ;
#19379=CARTESIAN_POINT ( 'NONE',  ( 3.267597511969735802, 21.59432767039258394, -1.500000000000002220 ) ) ;
#19380=CARTESIAN_POINT ( 'NONE',  ( -52.61350461722388161, -23.48786465467240703, 11.44779295918255180 ) ) ;
#19381=CARTESIAN_POINT ( 'NONE',  ( -10.49914784070103124, -20.09245350529190688, 11.49999999999998934 ) ) ;
#19383=CARTESIAN_POINT ( 'NONE',  ( -35.62287095715004170, -24.82558206586143967, 1.605769216559445933 ) ) ;
#19384=CARTESIAN_POINT ( 'NONE',  ( 9.711643268838683341, -19.58466107313252635, -1.500000000000002220 ) ) ;
#19389=EDGE_LOOP ( 'NONE', ( #67819, #25256, #81920, #40454 ) ) ;
#19390=CARTESIAN_POINT ( 'NONE',  ( -32.52287095715006160, -23.72773821059535848, 11.05748984161097681 ) ) ;
#19392=CARTESIAN_POINT ( 'NONE',  ( -69.55126625704998844, -25.16221347177320666, 3.076695569926833684 ) ) ;
#19393=CARTESIAN_POINT ( 'NONE',  ( -110.5228709571500616, -23.48783264082477018, -1.443836473390086583 ) ) ;
#19394=CARTESIAN_POINT ( 'NONE',  ( -21.26230640008892792, -0.7210608269398429693, -1.500000000000002220 ) ) ;
#19395=CARTESIAN_POINT ( 'NONE',  ( -125.5228709571500616, -25.00182538069146077, 7.747789668545104647 ) ) ;
#19396=CARTESIAN_POINT ( 'NONE',  ( -26.36141581567544989, -24.97064619426896215, 3.275177712619341541 ) ) ;
#19398=CARTESIAN_POINT ( 'NONE',  ( -85.55307269276684679, -24.15503026093913519, -0.2815557561904480921 ) ) ;
#19399=CARTESIAN_POINT ( 'NONE',  ( -84.62287095715007013, -23.73934037231757443, 11.05740245334328620 ) ) ;
#19400=CARTESIAN_POINT ( 'NONE',  ( -79.62287095715004170, -23.47596703998600631, 11.44779298504227860 ) ) ;
#19401=EDGE_LOOP ( 'NONE', ( #128, #62644, #93221, #25838 ) ) ;
#19402=EDGE_CURVE ( 'NONE', #18934, #3335, #81009, .T. ) ;
#19403=CARTESIAN_POINT ( 'NONE',  ( -15.85469643196389278, -11.46343829903102396, 11.49999999999999645 ) ) ;
#19404=CARTESIAN_POINT ( 'NONE',  ( -108.5228709571500616, -23.47596703998600631, 11.44779298504228038 ) ) ;
#19407=CARTESIAN_POINT ( 'NONE',  ( -29.26213830025908180, -24.96129339002881409, 7.420498735244676958 ) ) ;
#19408=ORIENTED_EDGE ( 'NONE', *, *, #487, .T. ) ;
#19410=CARTESIAN_POINT ( 'NONE',  ( -78.52287095715006160, -23.47596703998600631, 11.44779298504228571 ) ) ;
#19411=CARTESIAN_POINT ( 'NONE',  ( -99.74640623490535063, -25.25095820245264733, 5.397458776702524830 ) ) ;
#19413=ADVANCED_FACE ( 'NONE', ( #53789 ), #15211, .T. ) ;
#19414=CARTESIAN_POINT ( 'NONE',  ( -109.6228709571500559, -23.47593901973091235, -1.443836447538999312 ) ) ;
#19415=CARTESIAN_POINT ( 'NONE',  ( -60.52287095715007581, -24.52232992886362695, 0.6492154411905999289 ) ) ;
#19416=CARTESIAN_POINT ( 'NONE',  ( 13.13437215454093199, 14.66711140016434278, -1.500000000000002220 ) ) ;
#19418=VERTEX_POINT ( 'NONE', #69001 ) ;
#19419=B_SPLINE_CURVE_WITH_KNOTS ( 'NONE', 3,
 ( #95931, #63000, #10197, #18312 ),
 .UNSPECIFIED., .F., .F.,
 ( 4, 4 ),
 ( 0.000000000000000000, 9.999999999998897304E-05 ),
 .UNSPECIFIED. ) ;
#19421=LINE ( 'NONE', #18917, #29409 ) ;
#19425=ORIENTED_EDGE ( 'NONE', *, *, #96289, .T. ) ;
#19426=CARTESIAN_POINT ( 'NONE',  ( -74.52287095715009002, -23.96127896941631974, -0.6493128931038065765 ) ) ;
#19427=CARTESIAN_POINT ( 'NONE',  ( -126.2228709571500644, -23.47593901973090524, -1.443836447538996204 ) ) ;
#19428=FACE_OUTER_BOUND ( 'NONE', #92845, .T. ) ;
#19429=CARTESIAN_POINT ( 'NONE',  ( -118.5893591438163526, -24.34968618360934300, 0.1864209137778906622 ) ) ;
#19430=CARTESIAN_POINT ( 'NONE',  ( -78.92810380439237861, -25.14083923594767356, 2.947789366383930520 ) ) ;
#19431=CARTESIAN_POINT ( 'NONE',  ( -76.22287095715006444, -23.47596703998600631, 11.44779298504227683 ) ) ;
#19432=LINE ( 'NONE', #73721, #4065 ) ;
#19433=CARTESIAN_POINT ( 'NONE',  ( 4.608267332293128682, -19.41724391825443874, 11.49999999999998934 ) ) ;
#19434=CARTESIAN_POINT ( 'NONE',  ( -0.09684473721908999633, -21.79626877218119319, 10.45301531419930896 ) ) ;
#19435=CARTESIAN_POINT ( 'NONE',  ( 9.006517291608927778, -17.75031788249398446, -1.500000000000002220 ) ) ;
#19436=ORIENTED_EDGE ( 'NONE', *, *, #47785, .T. ) ;
#19437=CARTESIAN_POINT ( 'NONE',  ( -71.52287095715009002, -24.50216790748204687, 0.6166512839542508395 ) ) ;
#19441=CARTESIAN_POINT ( 'NONE',  ( -20.31193019649481357, 4.361987795224258946, 11.49999999999999645 ) ) ;
#19442=CARTESIAN_POINT ( 'NONE',  ( -37.62287095715005592, -23.47593901973091235, -1.443836447539011525 ) ) ;
#19448=CARTESIAN_POINT ( 'NONE',  ( 17.32893120472914816, 10.46255702124672027, -1.500000000000002220 ) ) ;
#19449=CARTESIAN_POINT ( 'NONE',  ( -55.55620429048338593, -25.00158670708909270, 2.256160236439165967 ) ) ;
#19450=CARTESIAN_POINT ( 'NONE',  ( -53.62287095715005592, -24.64898659630528499, 1.056161002820821038 ) ) ;
#19454=CARTESIAN_POINT ( 'NONE',  ( -80.36322839271868190, -25.31553952166217414, 4.968560711380208161 ) ) ;
#19455=DIRECTION ( 'NONE',  ( -1.000000000000000000, -3.773278334444166432E-23, -8.201307841325785021E-29 ) ) ;
#19456=CARTESIAN_POINT ( 'NONE',  ( 9.011679573027636891, 17.89655708981447901, -1.500000000000002220 ) ) ;
#19457=CARTESIAN_POINT ( 'NONE',  ( -20.73700405699343463, 3.470425206167693233, 11.49999999999999645 ) ) ;
#19460=CARTESIAN_POINT ( 'NONE',  ( -17.89045161427552699, -12.92718102017995641, -1.500000000000002220 ) ) ;
#19461=B_SPLINE_CURVE_WITH_KNOTS ( 'NONE', 3,
 ( #32542, #63514, #9707, #94434 ),
 .UNSPECIFIED., .F., .F.,
 ( 4, 4 ),
 ( 0.5201573561134056334, 0.5291637873855210561 ),
 .UNSPECIFIED. ) ;
#19463=EDGE_CURVE ( 'NONE', #79914, #14468, #95369, .T. ) ;
#19465=CARTESIAN_POINT ( 'NONE',  ( -47.62287095715005592, -23.94994826722565762, -0.6494450866342735829 ) ) ;
#19470=AXIS2_PLACEMENT_3D ( 'NONE', #56565, #95607, #27097 ) ;
#19473=CARTESIAN_POINT ( 'NONE',  ( -81.52287095715006160, -23.47596703998600631, 11.44779298504228571 ) ) ;
#19475=CARTESIAN_POINT ( 'NONE',  ( -20.56140336115741718, 0.6910293267889283664, -1.500000000000002220 ) ) ;
#19476=CARTESIAN_POINT ( 'NONE',  ( 10.28227983848843152, -18.94921665015282031, 11.49999999999999645 ) ) ;
#19478=ORIENTED_EDGE ( 'NONE', *, *, #38773, .F. ) ;
#19481=CARTESIAN_POINT ( 'NONE',  ( -87.62287095715004170, -29.50250786944525672, 11.44777988621623344 ) ) ;
#19482=CARTESIAN_POINT ( 'NONE',  ( -20.85237562250380350, -7.973873963886685345, 11.49999999999998934 ) ) ;
#19483=CARTESIAN_POINT ( 'NONE',  ( -82.62287095715007013, -24.66019654487199375, 8.947790411086128159 ) ) ;
#19487=AXIS2_PLACEMENT_3D ( 'NONE', #57241, #57733, #95779 ) ;
#19489=VECTOR ( 'NONE', #43570, 1000.000000000000114 ) ;
#19491=CARTESIAN_POINT ( 'NONE',  ( 15.14581745102402088, -14.33592658440916523, -1.500000000000002220 ) ) ;
#19492=ORIENTED_EDGE ( 'NONE', *, *, #41328, .T. ) ;
#19495=ORIENTED_EDGE ( 'NONE', *, *, #80963, .T. ) ;
#19497=CARTESIAN_POINT ( 'NONE',  ( -51.07434835877342749, -25.29404817037084285, 4.468853319241254063 ) ) ;
#19498=CARTESIAN_POINT ( 'NONE',  ( 21.04674311342985860, -0.3259866984596996864, -1.500000000000002220 ) ) ;
#19500=VERTEX_POINT ( 'NONE', #13197 ) ;
#19501=CARTESIAN_POINT ( 'NONE',  ( -95.92287095715009571, -23.47593901973090880, -1.443836447538997314 ) ) ;
#19503=CARTESIAN_POINT ( 'NONE',  ( -120.6235064687828356, -25.00182538069146787, 7.747789668545044250 ) ) ;
#19504=CARTESIAN_POINT ( 'NONE',  ( -28.58953762381673158, -23.31696865966051391, -1.443835777057014047 ) ) ;
#19505=CARTESIAN_POINT ( 'NONE',  ( -84.22287095715007865, -23.47593901973090169, -1.443836447538996870 ) ) ;
#19506=CARTESIAN_POINT ( 'NONE',  ( -14.78470843206283902, -15.91074852019131924, -1.500000000000002220 ) ) ;
#19508=CARTESIAN_POINT ( 'NONE',  ( 20.70802603420765564, 8.137917507125113303, 11.49999999999999645 ) ) ;
#19509=EDGE_LOOP ( 'NONE', ( #31609, #20458, #8914, #91490 ) ) ;
#19510=CARTESIAN_POINT ( 'NONE',  ( -50.72223433783125301, -25.31441730805603285, 5.237078674425484692 ) ) ;
#19512=CARTESIAN_POINT ( 'NONE',  ( -100.6228709571500559, -23.47593901973091235, -1.443836447539001089 ) ) ;
#19513=EDGE_LOOP ( 'NONE', ( #28852, #14871, #4433, #84115 ) ) ;
#19514=CARTESIAN_POINT ( 'NONE',  ( -53.92287095715006018, -23.47593901973090169, -1.443836447538997980 ) ) ;
#19516=ORIENTED_EDGE ( 'NONE', *, *, #11877, .T. ) ;
#19518=CARTESIAN_POINT ( 'NONE',  ( -49.10647344728249664, -25.27836164187442236, 4.050120676592289470 ) ) ;
#19520=CARTESIAN_POINT ( 'NONE',  ( -46.22287095715005734, -23.47596703998600631, 11.44779298504227683 ) ) ;
#19521=ORIENTED_EDGE ( 'NONE', *, *, #43892, .F. ) ;
#19523=CARTESIAN_POINT ( 'NONE',  ( -130.5728709571500588, -24.54081503060122671, 9.556887179928187592 ) ) ;
#19524=CARTESIAN_POINT ( 'NONE',  ( 22.44084908143146251, -0.7541981612834567361, -1.500000000000002220 ) ) ;
#19525=VERTEX_POINT ( 'NONE', #23820 ) ;
#19526=CARTESIAN_POINT ( 'NONE',  ( -100.0561916307745491, -25.05145249402578500, 7.523995081915606065 ) ) ;
#19528=EDGE_CURVE ( 'NONE', #5224, #26794, #17718, .T. ) ;
#19530=CARTESIAN_POINT ( 'NONE',  ( -64.62287095715007013, -23.47596703998600631, 11.44779298504227683 ) ) ;
#19531=EDGE_CURVE ( 'NONE', #70011, #96235, #8102, .T. ) ;
#19532=CARTESIAN_POINT ( 'NONE',  ( -30.60160445864372747, -24.57215472537218304, 9.174899246800713115 ) ) ;
#19533=CARTESIAN_POINT ( 'NONE',  ( 19.03533760385612439, 4.641190475545474037, -1.500000000000002220 ) ) ;
#19534=EDGE_CURVE ( 'NONE', #37940, #55816, #82073, .T. ) ;
#19535=CARTESIAN_POINT ( 'NONE',  ( -46.52204141198475185, -23.48783264082476663, -1.443836473390096575 ) ) ;
#19537=CARTESIAN_POINT ( 'NONE',  ( -15.55086147716002110, 14.89234021980106881, -1.500000000000002220 ) ) ;
#19538=CARTESIAN_POINT ( 'NONE',  ( -121.6228709571500417, -23.48783264082478794, -1.443836473390058384 ) ) ;
#19539=EDGE_CURVE ( 'NONE', #41151, #87739, #22746, .T. ) ;
#19540=FACE_OUTER_BOUND ( 'NONE', #68258, .T. ) ;
#19541=LINE ( 'NONE', #81943, #29781 ) ;
#19542=VECTOR ( 'NONE', #46958, 1000.000000000000114 ) ;
#19544=CARTESIAN_POINT ( 'NONE',  ( 4.903590608199674072, 22.46510890469962263, -1.500000000000002220 ) ) ;
#19548=CARTESIAN_POINT ( 'NONE',  ( 6.297820759360134524, 19.07352124001985771, 11.49999999999999645 ) ) ;
#19549=FACE_OUTER_BOUND ( 'NONE', #41617, .T. ) ;
#19551=CARTESIAN_POINT ( 'NONE',  ( -34.62287095715005592, -29.50247984919015209, -1.443849546365062242 ) ) ;
#19553=EDGE_CURVE ( 'NONE', #18378, #4330, #65219, .T. ) ;
#19555=CARTESIAN_POINT ( 'NONE',  ( 11.68167410197319001, -16.05257874518773065, 11.49999999999998934 ) ) ;
#19556=CARTESIAN_POINT ( 'NONE',  ( -113.5892054360595722, -24.34968618360934300, 0.1864209137778879699 ) ) ;
#19557=CARTESIAN_POINT ( 'NONE',  ( 19.69511366699831001, -0.05742560045514189665, -1.500000000000002220 ) ) ;
#19565=CARTESIAN_POINT ( 'NONE',  ( -15.40095275084150117, -13.70674696055758801, 11.49999999999999645 ) ) ;
#19566=CARTESIAN_POINT ( 'NONE',  ( -33.58953762381672448, -23.47596703998600276, 11.44779298504227505 ) ) ;
#19567=B_SPLINE_CURVE_WITH_KNOTS ( 'NONE', 3,
 ( #37960, #61318, #53705, #15123, #77006, #38462 ),
 .UNSPECIFIED., .F., .F.,
 ( 4, 2, 4 ),
 ( 1.570755371634454886E-05, 0.001396183895866091439, 0.002776660238015838614 ),
 .UNSPECIFIED. ) ;
#19568=CARTESIAN_POINT ( 'NONE',  ( 9.629844747126790949, -20.51516216672183290, 11.49999999999999645 ) ) ;
#19570=CARTESIAN_POINT ( 'NONE',  ( -69.38174606678134637, -25.12219007809040505, 6.471609302863886803 ) ) ;
#19574=DIRECTION ( 'NONE',  ( 0.000000000000000000, -2.173523156925979552E-06, 0.9999999999976378895 ) ) ;
#19575=ORIENTED_EDGE ( 'NONE', *, *, #45542, .T. ) ;
#19577=CARTESIAN_POINT ( 'NONE',  ( -99.29843613443789252, -25.24457243405052509, 6.219452043175907718 ) ) ;
#19578=CARTESIAN_POINT ( 'NONE',  ( -4.526818761702180893, -22.41603498850323817, -1.500000000000002220 ) ) ;
#19580=CARTESIAN_POINT ( 'NONE',  ( 20.63042821663210091, 6.393326493806346100, -1.500000000000002220 ) ) ;
#19581=CARTESIAN_POINT ( 'NONE',  ( -113.6244772655058739, -24.51419770103157347, 9.386484678747168076 ) ) ;
#19582=CARTESIAN_POINT ( 'NONE',  ( -76.52287095715007581, -23.48786465467241769, 11.44779295918254469 ) ) ;
#19583=CARTESIAN_POINT ( 'NONE',  ( -22.36795837939145670, 2.692536522722862813, 11.49999999999999645 ) ) ;
#19584=ORIENTED_EDGE ( 'NONE', *, *, #81750, .F. ) ;
#19585=CARTESIAN_POINT ( 'NONE',  ( -43.63416939196337552, -24.34968618360933590, 0.1864209137778851388 ) ) ;
#19586=CARTESIAN_POINT ( 'NONE',  ( 18.29167757401336303, -12.14499471347784798, -1.500000000000002220 ) ) ;
#19587=CARTESIAN_POINT ( 'NONE',  ( -44.56061661862030832, -23.73791477778911130, 11.05961554403171121 ) ) ;
#19588=DIRECTION ( 'NONE',  ( 0.000000000000000000, 0.9999999999976377785, 2.173523156925979128E-06 ) ) ;
#19589=ORIENTED_EDGE ( 'NONE', *, *, #22920, .T. ) ;
#19590=DIRECTION ( 'NONE',  ( 0.000000000000000000, 2.173523156925980399E-06, -0.9999999999976378895 ) ) ;
#19591=ADVANCED_FACE ( 'NONE', ( #2000 ), #24818, .T. ) ;
#19593=ORIENTED_EDGE ( 'NONE', *, *, #52797, .T. ) ;
#19598=CARTESIAN_POINT ( 'NONE',  ( -49.53224087187288660, -25.30395130311601193, 5.541308293284908260 ) ) ;
#19600=CARTESIAN_POINT ( 'NONE',  ( -104.6235422597730036, -24.66019654487200441, 8.947790411086108620 ) ) ;
#19601=CARTESIAN_POINT ( 'NONE',  ( -9.549598871097368047, 18.00506641634745009, -1.500000000000002220 ) ) ;
#19604=CARTESIAN_POINT ( 'NONE',  ( -71.66622694754684630, -25.20680239340841311, 6.551726662353233976 ) ) ;
#19605=CARTESIAN_POINT ( 'NONE',  ( -50.70418202325330270, -25.12629190293465697, 2.864576727199638295 ) ) ;
#19607=CARTESIAN_POINT ( 'NONE',  ( -105.5156730399040441, -24.15503026093913519, -0.2815557561904565298 ) ) ;
#19608=CARTESIAN_POINT ( 'NONE',  ( -71.53177174497976409, -25.03149702581040614, 6.885843724247062703 ) ) ;
#19610=CARTESIAN_POINT ( 'NONE',  ( -27.89567495842467082, -24.76880856562122801, 2.285879846231543500 ) ) ;
#19611=CARTESIAN_POINT ( 'NONE',  ( -107.6228709571500701, -29.50248528299804818, 1.056150453629043584 ) ) ;
#19612=B_SPLINE_CURVE_WITH_KNOTS ( 'NONE', 3,
 ( #67974, #6559, #23265, #13654 ),
 .UNSPECIFIED., .F., .F.,
 ( 4, 4 ),
 ( 0.000000000000000000, 9.999999999998897304E-05 ),
 .UNSPECIFIED. ) ;
#19614=CARTESIAN_POINT ( 'NONE',  ( 8.872108392497455753, -18.76566404461018678, -1.500000000000002220 ) ) ;
#19615=AXIS2_PLACEMENT_3D ( 'NONE', #65623, #49892, #95545 ) ;
#19618=PLANE ( 'NONE',  #16672 ) ;
#19619=ORIENTED_EDGE ( 'NONE', *, *, #60438, .T. ) ;
#19620=CARTESIAN_POINT ( 'NONE',  ( -41.51335775656676930, -23.73791477778911485, 11.05961554403170766 ) ) ;
#19621=CARTESIAN_POINT ( 'NONE',  ( -105.5228709571500616, -24.99156044556202971, 7.747789690856173195 ) ) ;
#19622=VERTEX_POINT ( 'NONE', #16711 ) ;
#19623=ORIENTED_EDGE ( 'NONE', *, *, #15326, .F. ) ;
#19624=CARTESIAN_POINT ( 'NONE',  ( -114.6228709571500843, -24.34917612406838217, 0.1852690917426682848 ) ) ;
#19627=CARTESIAN_POINT ( 'NONE',  ( -43.64732276058348504, -23.96169478059712432, 10.65365249895718769 ) ) ;
#19628=CARTESIAN_POINT ( 'NONE',  ( 12.17348956504948987, -18.45705692928949659, 11.49999999999999645 ) ) ;
#19630=CARTESIAN_POINT ( 'NONE',  ( -108.5164791698326070, -24.15543982623908192, -0.2315651400026445539 ) ) ;
#19631=CARTESIAN_POINT ( 'NONE',  ( 19.70651319644445465, -11.07993823016455792, -1.500000000000002220 ) ) ;
#19634=AXIS2_PLACEMENT_3D ( 'NONE', #55122, #40393, #1835 ) ;
#19637=CARTESIAN_POINT ( 'NONE',  ( -69.52287095715006160, -23.47593901973090169, -1.443836447538996870 ) ) ;
#19638=CARTESIAN_POINT ( 'NONE',  ( -128.5228709571500474, -23.48783264083417066, -1.443836473375472274 ) ) ;
#19639=ORIENTED_EDGE ( 'NONE', *, *, #43489, .F. ) ;
#19640=CARTESIAN_POINT ( 'NONE',  ( 13.39648796734645231, 16.42122281929413319, -1.500000000000002220 ) ) ;
#19641=B_SPLINE_CURVE_WITH_KNOTS ( 'NONE', 3,
 ( #13425, #81463, #67742, #20537 ),
 .UNSPECIFIED., .F., .F.,
 ( 4, 4 ),
 ( 0.000000000000000000, 0.0004038461538461435296 ),
 .UNSPECIFIED. ) ;
#19643=CARTESIAN_POINT ( 'NONE',  ( -41.86995616089613748, -25.27977532709532227, 4.210709737483026238 ) ) ;
#19644=CARTESIAN_POINT ( 'NONE',  ( 21.15698459081360383, -7.064864530413820454, -1.500000000000002220 ) ) ;
#19645=CARTESIAN_POINT ( 'NONE',  ( -50.22356044790234364, -25.03220905709108735, 7.558303196641526611 ) ) ;
#19646=VERTEX_POINT ( 'NONE', #47677 ) ;
#19648=CARTESIAN_POINT ( 'NONE',  ( -37.62372550051912157, -24.65952944569304606, 1.056160979905695907 ) ) ;
#19649=CARTESIAN_POINT ( 'NONE',  ( -111.5228709571500616, -24.65952944569305316, 1.056160979905704123 ) ) ;
#19651=CARTESIAN_POINT ( 'NONE',  ( -17.64752530894654470, 8.349842952099315596, 11.49999999999998934 ) ) ;
#19652=EDGE_CURVE ( 'NONE', #41451, #56734, #49383, .T. ) ;
#19653=CARTESIAN_POINT ( 'NONE',  ( 21.36505145794347982, 1.902718533054148509, -1.500000000000002220 ) ) ;
#19656=PLANE ( 'NONE',  #16302 ) ;
#19657=CARTESIAN_POINT ( 'NONE',  ( -58.52287095715004739, -23.47593901973090169, -1.443836447538997092 ) ) ;
#19658=CARTESIAN_POINT ( 'NONE',  ( -0.9122204482399535186, 22.77315974801211240, -1.500000000000002220 ) ) ;
#19660=FACE_OUTER_BOUND ( 'NONE', #13627, .T. ) ;
#19662=CARTESIAN_POINT ( 'NONE',  ( 19.92730240972663935, 0.8534881809820089593, 11.49999999999999645 ) ) ;
#19663=CARTESIAN_POINT ( 'NONE',  ( -78.58953762381671027, -24.64898659630367916, 1.056161002820386274 ) ) ;
#19664=CARTESIAN_POINT ( 'NONE',  ( -39.60861305632572282, -23.73791477778911485, 11.05961554403170943 ) ) ;
#19666=ORIENTED_EDGE ( 'NONE', *, *, #34891, .F. ) ;
#19667=EDGE_CURVE ( 'NONE', #75111, #28349, #37336, .T. ) ;
#19670=CARTESIAN_POINT ( 'NONE',  ( 15.89274262425319861, 14.76810421718133171, 11.49999999999998934 ) ) ;
#19672=CARTESIAN_POINT ( 'NONE',  ( 17.64699390344983598, -8.409456921668478913, -1.500000000000002220 ) ) ;
#19673=CARTESIAN_POINT ( 'NONE',  ( -55.57062048815932087, -23.48786465467241413, 11.44779295918254647 ) ) ;
#19676=CARTESIAN_POINT ( 'NONE',  ( 13.86372479123709311, 15.02075200336711092, 11.49999999999999645 ) ) ;
#19677=CARTESIAN_POINT ( 'NONE',  ( -50.04514766445114304, -25.30330263116561440, 5.239125874704871677 ) ) ;
#19678=AXIS2_PLACEMENT_3D ( 'NONE', #59632, #30156, #14924 ) ;
#19680=ORIENTED_EDGE ( 'NONE', *, *, #92916, .F. ) ;
#19681=PLANE ( 'NONE',  #32963 ) ;
#19682=DIRECTION ( 'NONE',  ( -3.773278334453080206E-23, 0.9999999999976377785, 2.173523156925979975E-06 ) ) ;
#19684=LINE ( 'NONE', #43545, #1421 ) ;
#19687=EDGE_CURVE ( 'NONE', #97228, #73442, #77194, .T. ) ;
#19688=VECTOR ( 'NONE', #4966, 1000.000000000000114 ) ;
#19689=CARTESIAN_POINT ( 'NONE',  ( 13.47786528765806580, -18.65256936556403744, 11.49999999999999645 ) ) ;
#19690=CARTESIAN_POINT ( 'NONE',  ( -17.51746294255814718, -14.55262482891283504, -1.500000000000002220 ) ) ;
#19691=CARTESIAN_POINT ( 'NONE',  ( -110.5228709571500616, -24.99132157543167310, 2.256160258750667502 ) ) ;
#19692=CARTESIAN_POINT ( 'NONE',  ( -33.52287095715006160, -24.64898659630367206, 1.056161002820817485 ) ) ;
#19693=CARTESIAN_POINT ( 'NONE',  ( -120.5228709571500900, -23.84081130425355965, 10.88220057483161263 ) ) ;
#19696=CARTESIAN_POINT ( 'NONE',  ( -110.5222005161765679, -23.48783264082476308, -1.443836473390091468 ) ) ;
#19697=CARTESIAN_POINT ( 'NONE',  ( 1.740910633133015972, 21.82039641801506846, 11.49999999999998934 ) ) ;
#19698=EDGE_CURVE ( 'NONE', #95505, #79014, #5873, .T. ) ;
#19701=CARTESIAN_POINT ( 'NONE',  ( -28.62287095715004881, -29.50250473134420659, 10.00399446418115268 ) ) ;
#19704=CARTESIAN_POINT ( 'NONE',  ( -5.688044216684545518, -19.60349290560521140, -1.500000000000002220 ) ) ;
#19707=ORIENTED_EDGE ( 'NONE', *, *, #9937, .F. ) ;
#19709=CARTESIAN_POINT ( 'NONE',  ( 20.35648204094723468, -10.72454223111430593, -1.500000000000002220 ) ) ;
#19710=CARTESIAN_POINT ( 'NONE',  ( -80.52287095715003318, -24.15431212366389957, -0.2830839119429247042 ) ) ;
#19711=CARTESIAN_POINT ( 'NONE',  ( 18.82035724208558491, -7.196742317222773799, -1.500000000000002220 ) ) ;
#19712=VERTEX_POINT ( 'NONE', #80610 ) ;
#19715=DIRECTION ( 'NONE',  ( 0.000000000000000000, -0.9999999999976377785, -2.173523156925979128E-06 ) ) ;
#19717=CARTESIAN_POINT ( 'NONE',  ( -17.20161093224466953, -12.68000408521323408, 11.49999999999999645 ) ) ;
#19719=DIRECTION ( 'NONE',  ( 0.000000000000000000, 0.9999999999976377785, 2.173523156925979975E-06 ) ) ;
#19721=CARTESIAN_POINT ( 'NONE',  ( -19.27636426328722763, -11.15942449563467775, -1.500000000000002220 ) ) ;
#19722=CARTESIAN_POINT ( 'NONE',  ( -20.51892249978613236, 2.527598752449112585, -1.500000000000002220 ) ) ;
#19724=ORIENTED_EDGE ( 'NONE', *, *, #55449, .T. ) ;
#19726=DIRECTION ( 'NONE',  ( -3.773278334453079030E-23, 0.9999999999976377785, 2.173523156925979128E-06 ) ) ;
#19727=ORIENTED_EDGE ( 'NONE', *, *, #48272, .T. ) ;
#19729=ORIENTED_EDGE ( 'NONE', *, *, #3162, .F. ) ;
#19731=CARTESIAN_POINT ( 'NONE',  ( 20.89173079421859214, 1.537965369061287557, -1.500000000000002220 ) ) ;
#19732=CARTESIAN_POINT ( 'NONE',  ( 20.64021973274467570, 7.317367941133321452, 11.49999999999999645 ) ) ;
#19734=CARTESIAN_POINT ( 'NONE',  ( -16.74547196562220464, 15.07928529822544661, -1.500000000000002220 ) ) ;
#19735=EDGE_CURVE ( 'NONE', #65316, #10349, #13048, .T. ) ;
#19736=CARTESIAN_POINT ( 'NONE',  ( 0.7041596644206948863, -20.94928778062849162, 11.49999999999998934 ) ) ;
#19737=CARTESIAN_POINT ( 'NONE',  ( -110.5228709571500048, -24.51163499207180152, 0.6490370598555574855 ) ) ;
#19739=CARTESIAN_POINT ( 'NONE',  ( -114.5228709571500616, -23.48783264083396105, -1.443836473375806895 ) ) ;
#19740=CARTESIAN_POINT ( 'NONE',  ( -31.66446019296015280, -24.87219037988794312, 1.747789950295620232 ) ) ;
#19742=VERTEX_POINT ( 'NONE', #11100 ) ;
#19743=VERTEX_POINT ( 'NONE', #42069 ) ;
#19747=CARTESIAN_POINT ( 'NONE',  ( 1.049947104896167049, -21.43676768134831434, -1.500000000000002220 ) ) ;
#19750=CARTESIAN_POINT ( 'NONE',  ( 11.82777538550527119, 17.46297031709455183, 11.49999999999998934 ) ) ;
#19752=CARTESIAN_POINT ( 'NONE',  ( -67.62287095715005592, -24.64898659630367916, 1.056161002820824368 ) ) ;
#19753=CARTESIAN_POINT ( 'NONE',  ( -50.64239288538053074, -24.40133493613049964, 9.663955038902802386 ) ) ;
#19754=CARTESIAN_POINT ( 'NONE',  ( -101.6235504250154236, -24.65952944569305316, 1.056160979905706121 ) ) ;
#19755=CARTESIAN_POINT ( 'NONE',  ( -109.3611003627813147, -25.29407500041303791, 4.275929869372101955 ) ) ;
#19756=CARTESIAN_POINT ( 'NONE',  ( -21.55788180805707555, 4.768121097544787190, -1.500000000000002220 ) ) ;
#19758=ADVANCED_FACE ( 'NONE', ( #3997 ), #96337, .F. ) ;
#19759=DIRECTION ( 'NONE',  ( 0.000000000000000000, 0.9999999999976377785, 2.173523156925979975E-06 ) ) ;
#19760=EDGE_CURVE ( 'NONE', #62593, #88005, #72381, .T. ) ;
#19762=CARTESIAN_POINT ( 'NONE',  ( -51.91911984596691809, -25.31633312187877394, 5.987871665635145391 ) ) ;
#19763=CARTESIAN_POINT ( 'NONE',  ( -41.81544514806834201, -25.27955868049266996, 4.607988218795668445 ) ) ;
#19764=CARTESIAN_POINT ( 'NONE',  ( -62.62750437465097519, -24.51419770103156281, 9.386484678747184063 ) ) ;
#19767=CARTESIAN_POINT ( 'NONE',  ( -96.62287095715007013, -23.73934037231757088, 11.05740245334328975 ) ) ;
#19768=CARTESIAN_POINT ( 'NONE',  ( 16.11712757473013014, 13.99349609535929773, 11.49999999999998934 ) ) ;
#19773=CARTESIAN_POINT ( 'NONE',  ( -81.23220280989026776, -25.17055267398807317, 6.810866775833154030 ) ) ;
#19774=CARTESIAN_POINT ( 'NONE',  ( -9.675873947287982446, 20.46574270456686406, -1.500000000000002220 ) ) ;
#19775=ADVANCED_FACE ( 'NONE', ( #81110 ), #2924, .T. ) ;
#19779=CARTESIAN_POINT ( 'NONE',  ( -99.52287095715009002, -23.47593901973090524, -1.443836447538996648 ) ) ;
#19780=CARTESIAN_POINT ( 'NONE',  ( -17.81549539028256746, -8.563599010019245839, 11.49999999999999645 ) ) ;
#19781=CARTESIAN_POINT ( 'NONE',  ( -82.62287095715005592, -23.95044443724992789, 10.65354141964649592 ) ) ;
#19782=CARTESIAN_POINT ( 'NONE',  ( -32.07722060962683486, -25.27409513349664749, 3.734526454214742497 ) ) ;
#19783=EDGE_LOOP ( 'NONE', ( #25832, #26085, #3305, #25963 ) ) ;
#19786=CARTESIAN_POINT ( 'NONE',  ( -70.52287095715007581, -24.83620972994590659, 8.398175272781360334 ) ) ;
#19787=CARTESIAN_POINT ( 'NONE',  ( -102.6228709571500559, -24.64898659630368272, 1.056161002820829697 ) ) ;
#19788=CARTESIAN_POINT ( 'NONE',  ( -15.70146493180990888, -14.86199287721409590, -1.500000000000002220 ) ) ;
#19790=CARTESIAN_POINT ( 'NONE',  ( -18.23339674026497903, -6.527145932826366348, -1.500000000000002220 ) ) ;
#19791=EDGE_CURVE ( 'NONE', #46870, #45965, #26362, .T. ) ;
#19792=B_SPLINE_CURVE_WITH_KNOTS ( 'NONE', 3,
 ( #57706, #89146, #3922, #81538, #25235, #96259 ),
 .UNSPECIFIED., .F., .F.,
 ( 4, 2, 4 ),
 ( 1.570755371634013412E-05, 0.001396183895866087536, 0.002776660238015834711 ),
 .UNSPECIFIED. ) ;
#19793=FACE_OUTER_BOUND ( 'NONE', #18006, .T. ) ;
#19795=CARTESIAN_POINT ( 'NONE',  ( -18.77405512783484198, 6.205181830411797606, -1.500000000000002220 ) ) ;
#19797=CARTESIAN_POINT ( 'NONE',  ( 2.300710779914242110, 20.15441874099239783, 11.49999999999999645 ) ) ;
#19798=CARTESIAN_POINT ( 'NONE',  ( -119.5228709571500474, -23.73934037231757799, 11.05740245334328087 ) ) ;
#19799=CARTESIAN_POINT ( 'NONE',  ( -51.62287095715005592, -29.50248528299804818, 1.056150453629033370 ) ) ;
#19801=ORIENTED_EDGE ( 'NONE', *, *, #45987, .F. ) ;
#19805=CARTESIAN_POINT ( 'NONE',  ( -92.58953762381672448, -24.66019654487199730, 8.947790411086121054 ) ) ;
#19806=CARTESIAN_POINT ( 'NONE',  ( -86.92287095715003886, -23.47596703998600276, 11.44779298504227683 ) ) ;
#19807=CARTESIAN_POINT ( 'NONE',  ( 11.39338536883839659, -16.50304575528446804, 11.49999999999998934 ) ) ;
#19808=CARTESIAN_POINT ( 'NONE',  ( -126.5228709571500616, -24.64965694238408034, 8.947790433994189385 ) ) ;
#19809=ORIENTED_EDGE ( 'NONE', *, *, #79470, .T. ) ;
#19810=CARTESIAN_POINT ( 'NONE',  ( -58.55620429048338593, -24.66019654487199020, 8.947790411086135265 ) ) ;
#19811=AXIS2_PLACEMENT_3D ( 'NONE', #3850, #34790, #65761 ) ;
#19817=EDGE_CURVE ( 'NONE', #59400, #27745, #96625, .T. ) ;
#19818=DIRECTION ( 'NONE',  ( -0.000000000000000000, 2.173523156925979552E-06, -0.9999999999976378895 ) ) ;
#19820=CARTESIAN_POINT ( 'NONE',  ( -12.25758032491116367, 16.21837406056298292, 11.49999999999998934 ) ) ;
#19821=ORIENTED_EDGE ( 'NONE', *, *, #83621, .F. ) ;
#19822=CARTESIAN_POINT ( 'NONE',  ( 2.319610639010541764, -22.79860127089448696, 11.49999999999998934 ) ) ;
#19824=ORIENTED_EDGE ( 'NONE', *, *, #36573, .F. ) ;
#19825=CARTESIAN_POINT ( 'NONE',  ( -49.34131120686307526, -25.30051202764760632, 4.642102575841966505 ) ) ;
#19826=CARTESIAN_POINT ( 'NONE',  ( -49.66108014839032592, -25.26264131307726757, 6.884432116491313813 ) ) ;
#19827=VECTOR ( 'NONE', #60983, 1000.000000000000114 ) ;
#19828=CARTESIAN_POINT ( 'NONE',  ( -72.58953762381672448, -23.47593901973091235, -1.443836447539006196 ) ) ;
#19829=CARTESIAN_POINT ( 'NONE',  ( 20.83148622972472808, -3.941400823363257366, 11.49999999999999645 ) ) ;
#19831=CARTESIAN_POINT ( 'NONE',  ( -15.97456084408017674, 15.39233244482803009, 11.49999999999998934 ) ) ;
#19832=CARTESIAN_POINT ( 'NONE',  ( 20.45670835789597319, 2.398913822417158226, -1.500000000000002220 ) ) ;
#19833=ADVANCED_FACE ( 'NONE', ( #52161 ), #87972, .T. ) ;
#19834=ORIENTED_EDGE ( 'NONE', *, *, #63480, .T. ) ;
#19835=CARTESIAN_POINT ( 'NONE',  ( -41.65560179646217165, -23.73766607897670866, -1.055555164236441801 ) ) ;
#19836=ORIENTED_EDGE ( 'NONE', *, *, #72506, .T. ) ;
#19838=CARTESIAN_POINT ( 'NONE',  ( -126.6228709571500843, -24.66019654487200441, 8.947790411086119278 ) ) ;
#19839=ORIENTED_EDGE ( 'NONE', *, *, #95018, .T. ) ;
#19840=VERTEX_POINT ( 'NONE', #83091 ) ;
#19841=EDGE_CURVE ( 'NONE', #89121, #72949, #13581, .T. ) ;
#19842=ORIENTED_EDGE ( 'NONE', *, *, #71223, .F. ) ;
#19843=VECTOR ( 'NONE', #33106, 1000.000000000000114 ) ;
#19844=CARTESIAN_POINT ( 'NONE',  ( -71.20541289166536103, -29.50249360700573931, 4.885880847770192048 ) ) ;
#19845=DIRECTION ( 'NONE',  ( 0.000000000000000000, -0.9999999999976377785, -2.173523156925979128E-06 ) ) ;
#19846=CARTESIAN_POINT ( 'NONE',  ( -94.55620429048336462, -24.64965694238574656, 8.947790433994196491 ) ) ;
#19847=CARTESIAN_POINT ( 'NONE',  ( 10.87737074370964407, 17.65887017642603851, -1.500000000000002220 ) ) ;
#19848=CARTESIAN_POINT ( 'NONE',  ( 18.95625057990686813, 10.65820999021175730, 11.49999999999999645 ) ) ;
#19849=ORIENTED_EDGE ( 'NONE', *, *, #84965, .T. ) ;
#19850=EDGE_CURVE ( 'NONE', #14468, #36980, #20411, .T. ) ;
#19852=CARTESIAN_POINT ( 'NONE',  ( -119.6228709571501128, -24.35013146730203815, 9.818937971375104823 ) ) ;
#19853=CARTESIAN_POINT ( 'NONE',  ( 20.43785579724129420, 9.289222182981756504, -1.500000000000002220 ) ) ;
#19855=ADVANCED_FACE ( 'NONE', ( #8978 ), #38430, .F. ) ;
#19859=CARTESIAN_POINT ( 'NONE',  ( -75.52287095715006160, -24.14321612903116332, -0.2833117244521500266 ) ) ;
#19860=FACE_OUTER_BOUND ( 'NONE', #45985, .T. ) ;
#19862=EDGE_CURVE ( 'NONE', #13321, #39067, #56765, .T. ) ;
#19863=ORIENTED_EDGE ( 'NONE', *, *, #100264, .T. ) ;
#19865=CARTESIAN_POINT ( 'NONE',  ( -46.48369806289436923, -24.66019654487199375, 8.947790411086122830 ) ) ;
#19866=VERTEX_POINT ( 'NONE', #46056 ) ;
#19867=VECTOR ( 'NONE', #36626, 1000.000000000000114 ) ;
#19868=CARTESIAN_POINT ( 'NONE',  ( 12.11089201280794470, -17.53110042540249225, -1.500000000000002220 ) ) ;
#19869=ORIENTED_EDGE ( 'NONE', *, *, #1374, .T. ) ;
#19870=CARTESIAN_POINT ( 'NONE',  ( -88.59161115057158042, -24.15543982623907837, -0.2315651400026634832 ) ) ;
#19871=CARTESIAN_POINT ( 'NONE',  ( 21.07893183998518438, -5.767110019903106455, -1.500000000000002220 ) ) ;
#19873=CARTESIAN_POINT ( 'NONE',  ( 20.21490908150494192, 10.32750977814155391, -1.500000000000002220 ) ) ;
#19874=CARTESIAN_POINT ( 'NONE',  ( -41.42599659256448774, -25.28892559315755761, 3.925284093188281087 ) ) ;
#19875=CARTESIAN_POINT ( 'NONE',  ( -35.62287095715004881, -24.62226745350438506, 0.9660975649728152925 ) ) ;
#19876=CARTESIAN_POINT ( 'NONE',  ( 11.39931579351042679, 18.75040340349860557, -1.500000000000002220 ) ) ;
#19878=ORIENTED_EDGE ( 'NONE', *, *, #16253, .F. ) ;
#19879=FACE_OUTER_BOUND ( 'NONE', #35725, .T. ) ;
#19886=VECTOR ( 'NONE', #13426, 1000.000000000000114 ) ;
#19887=CARTESIAN_POINT ( 'NONE',  ( -40.48848937406284421, -25.17730189479833669, 6.892737719230496829 ) ) ;
#19888=CARTESIAN_POINT ( 'NONE',  ( -10.24013151130244736, -23.09176648418334921, 1.095224832288505201 ) ) ;
#19889=CARTESIAN_POINT ( 'NONE',  ( -21.25539211000977957, 0.9166567589900279645, -1.500000000000002220 ) ) ;
#19890=CARTESIAN_POINT ( 'NONE',  ( -112.5139921198612711, -24.65952944569305316, 1.056160979905707675 ) ) ;
#19891=CARTESIAN_POINT ( 'NONE',  ( -26.14706027629300422, -24.75186366296204454, 4.097425152336787058 ) ) ;
#19892=EDGE_CURVE ( 'NONE', #90405, #49749, #40921, .T. ) ;
#19893=CARTESIAN_POINT ( 'NONE',  ( -85.58094847593091004, -25.00158670708910691, 2.256160236439219258 ) ) ;
#19894=CARTESIAN_POINT ( 'NONE',  ( -68.50597231294825917, -24.15543982623907127, -0.2315651400026649820 ) ) ;
#19895=ADVANCED_FACE ( 'NONE', ( #23693 ), #15089, .F. ) ;
#19896=CARTESIAN_POINT ( 'NONE',  ( -39.62287095715005592, -23.48786465467240347, 11.44779295918255180 ) ) ;
#19898=CARTESIAN_POINT ( 'NONE',  ( -13.18904525526904692, 14.46673508071025971, 11.49999999999999645 ) ) ;
#19899=CARTESIAN_POINT ( 'NONE',  ( -99.12380231474227799, -25.27434709648489886, 4.001575133896465353 ) ) ;
#19900=PLANE ( 'NONE',  #15602 ) ;
#19901=ORIENTED_EDGE ( 'NONE', *, *, #87757, .T. ) ;
#19902=EDGE_CURVE ( 'NONE', #93720, #14489, #70030, .T. ) ;
#19904=CARTESIAN_POINT ( 'NONE',  ( -99.16166289166532977, -25.31166538673566180, 5.311370725864150266 ) ) ;
#19905=DIRECTION ( 'NONE',  ( 0.000000000000000000, -0.9999999999976377785, -2.173523156925979128E-06 ) ) ;
#19907=VECTOR ( 'NONE', #81334, 1000.000000000000114 ) ;
#19908=CARTESIAN_POINT ( 'NONE',  ( -40.62287095715004170, -24.14406661707770141, 10.28769366152061160 ) ) ;
#19909=CARTESIAN_POINT ( 'NONE',  ( 17.62393913918218402, -8.800128315780904487, -1.500000000000002220 ) ) ;
#19910=ADVANCED_FACE ( 'NONE', ( #47557 ), #9331, .T. ) ;
#19914=CARTESIAN_POINT ( 'NONE',  ( -114.6228709571500559, -29.50250243563736774, 8.947779886222136270 ) ) ;
#19915=B_SPLINE_CURVE_WITH_KNOTS ( 'NONE', 3,
 ( #2277, #3773, #63685, #10876 ),
 .UNSPECIFIED., .F., .F.,
 ( 4, 4 ),
 ( 1.798233777275264259E-11, 0.002370364882941363924 ),
 .UNSPECIFIED. ) ;
#19918=EDGE_CURVE ( 'NONE', #10895, #15452, #51892, .T. ) ;
#19919=EDGE_LOOP ( 'NONE', ( #44964, #50286, #97124, #89606 ) ) ;
#19921=CARTESIAN_POINT ( 'NONE',  ( -105.6228709571501128, -24.82576562982392687, 8.398263435472967942 ) ) ;
#19922=CARTESIAN_POINT ( 'NONE',  ( -47.54695344001475377, -24.15543982623907127, -0.2315651400026536022 ) ) ;
#19923=CARTESIAN_POINT ( 'NONE',  ( -84.52287095715006160, -23.47596703998600631, 11.44779298504228571 ) ) ;
#19926=VECTOR ( 'NONE', #27140, 1000.000000000000114 ) ;
#19927=CARTESIAN_POINT ( 'NONE',  ( -117.5228709571500758, -29.50250243563736774, 8.947779886222134493 ) ) ;
#19928=CARTESIAN_POINT ( 'NONE',  ( 17.47191945374660094, 9.613082372698542599, 11.49999999999998934 ) ) ;
#19930=CARTESIAN_POINT ( 'NONE',  ( -0.05005869551267223827, -22.40195084843249518, 1.075460532450188023 ) ) ;
#19936=CARTESIAN_POINT ( 'NONE',  ( -125.6228709571500559, -29.50250786944525672, 11.44777988621622633 ) ) ;
#19938=CARTESIAN_POINT ( 'NONE',  ( -26.11702346598058710, -24.95514697357233302, 4.364016039383404433 ) ) ;
#19940=ORIENTED_EDGE ( 'NONE', *, *, #47500, .T. ) ;
#19941=B_SPLINE_SURFACE_WITH_KNOTS ( 'NONE', 3, 1, ( 
 ( #83891, #37229 ),
 ( #7768, #14873 ),
 ( #9652, #40609 ),
 ( #91500, #29107 ),
 ( #86770, #14373 ),
 ( #21979, #30102 ),
 ( #30604, #68181 ),
 ( #94383, #60083 ),
 ( #29604, #76271 ),
 ( #52960, #6765 ),
 ( #100090, #92003 ),
 ( #22473, #45841 ),
 ( #32489, #63462 ),
 ( #7260, #38214 ),
 ( #69170, #10656 ),
 ( #2056, #89277 ),
 ( #50222, #17768 ),
 ( #95388, #96386 ),
 ( #41113, #34494 ) ),
 .UNSPECIFIED., .F., .F., .F.,
 ( 4, 1, 1, 1, 1, 1, 1, 1, 1, 1, 1, 1, 1, 1, 1, 1, 4 ),
 ( 2, 2 ),
 ( 0.000000000000000000, 0.07607173695556672388, 0.1487517145745168301, 0.2184027938458466545, 0.2857595810623843602, 0.3505980236748781342, 0.4149640445981273573, 0.4780693385717832977, 0.5417606760069103577, 0.6043498585387204747, 0.6640750210708951107, 0.7214636230802008443, 0.7775871282364469339, 0.8326444469271317983, 0.8878435110684590459, 0.9434603426519472258, 1.000000000000000000 ),
 ( 0.000000000000000000, 1.000000000000000000 ),
 .UNSPECIFIED. ) ;
#19942=FACE_OUTER_BOUND ( 'NONE', #73063, .T. ) ;
#19945=CARTESIAN_POINT ( 'NONE',  ( 8.375906630400100639, -18.44307005126401933, -1.500000000000002220 ) ) ;
#19946=B_SPLINE_CURVE_WITH_KNOTS ( 'NONE', 3,
 ( #26192, #3377, #50530, #65781 ),
 .UNSPECIFIED., .F., .F.,
 ( 4, 4 ),
 ( 0.000000000000000000, 1.000000000000000000 ),
 .UNSPECIFIED. ) ;
#19947=DIRECTION ( 'NONE',  ( -3.773278334453079618E-23, 0.9999999999976377785, 2.173523156925979975E-06 ) ) ;
#19948=DIRECTION ( 'NONE',  ( 0.000000000000000000, -0.9999999999976377785, -2.173523156925979975E-06 ) ) ;
#19952=CARTESIAN_POINT ( 'NONE',  ( -80.09162780144649219, -25.31560333233622373, 5.003082748975755223 ) ) ;
#19954=CARTESIAN_POINT ( 'NONE',  ( 2.879247915899910470, -19.84986158617241614, -1.500000000000002220 ) ) ;
#19956=CARTESIAN_POINT ( 'NONE',  ( 14.98681507544721292, -14.71779577663021321, 11.49999999999999645 ) ) ;
#19959=CARTESIAN_POINT ( 'NONE',  ( 18.88560736741940005, 11.47387103136259690, 11.49999999999998934 ) ) ;
#19960=B_SPLINE_CURVE_WITH_KNOTS ( 'NONE', 3,
 ( #50907, #32807, #59024, #12821 ),
 .UNSPECIFIED., .F., .F.,
 ( 4, 4 ),
 ( 0.4401001892501570922, 0.4491066205222725150 ),
 .UNSPECIFIED. ) ;
#19961=CARTESIAN_POINT ( 'NONE',  ( -39.46140038746126777, -25.27805951068589962, 4.366343927290111893 ) ) ;
#19962=EDGE_CURVE ( 'NONE', #18378, #79772, #11979, .T. ) ;
#19963=CARTESIAN_POINT ( 'NONE',  ( -91.62287095715004170, -24.64965695001468404, 8.947790433994180503 ) ) ;
#19964=DIRECTION ( 'NONE',  ( -1.000000000000000000, -3.773278334444166432E-23, -8.201307841325785021E-29 ) ) ;
#19965=ORIENTED_EDGE ( 'NONE', *, *, #70456, .T. ) ;
#19966=CARTESIAN_POINT ( 'NONE',  ( -72.63060126349051870, -24.34968618360933590, 0.1864209137778795600 ) ) ;
#19968=EDGE_CURVE ( 'NONE', #95644, #82884, #88116, .T. ) ;
#19969=VERTEX_POINT ( 'NONE', #49560 ) ;
#19972=CARTESIAN_POINT ( 'NONE',  ( -49.52287095715006160, -24.64898659630367561, 1.056161002820821038 ) ) ;
#19974=CARTESIAN_POINT ( 'NONE',  ( -76.51216158835003966, -23.96119346886880663, -0.6495511937832058047 ) ) ;
#19975=CARTESIAN_POINT ( 'NONE',  ( -12.99546161633903552, -15.93940442571882876, -1.500000000000002220 ) ) ;
#19977=CARTESIAN_POINT ( 'NONE',  ( -21.01953065494444317, -4.859126342152997324, 11.49999999999999645 ) ) ;
#19978=VERTEX_POINT ( 'NONE', #80489 ) ;
#19979=CARTESIAN_POINT ( 'NONE',  ( -49.27764846858840997, -25.26180677598144086, 6.145204968850301874 ) ) ;
#19980=CARTESIAN_POINT ( 'NONE',  ( -56.52287095715008292, -24.66019654487199375, 8.947790411086122830 ) ) ;
#19982=CARTESIAN_POINT ( 'NONE',  ( -11.77839732991513166, 18.97803183815481987, -1.500000000000002220 ) ) ;
#19983=EDGE_CURVE ( 'NONE', #7232, #9237, #62673, .T. ) ;
#19985=AXIS2_PLACEMENT_3D ( 'NONE', #71194, #1685, #63091 ) ;
#19986=CARTESIAN_POINT ( 'NONE',  ( -59.62287095715002039, -24.51387760970724372, 9.387446482453427166 ) ) ;
#19987=CARTESIAN_POINT ( 'NONE',  ( -32.38277616518237778, -25.12026506542016335, 2.831122744435439209 ) ) ;
#19988=VERTEX_POINT ( 'NONE', #72894 ) ;
#19991=EDGE_CURVE ( 'NONE', #53340, #2549, #33740, .T. ) ;
#19992=CARTESIAN_POINT ( 'NONE',  ( -20.64841573231975147, 3.066018724555340746, 11.49999999999998934 ) ) ;
#19993=ORIENTED_EDGE ( 'NONE', *, *, #59871, .T. ) ;
#19995=ORIENTED_EDGE ( 'NONE', *, *, #73115, .T. ) ;
#19998=CARTESIAN_POINT ( 'NONE',  ( -100.5847584379934716, -24.92592662359561118, 8.075495903017998245 ) ) ;
#19999=CARTESIAN_POINT ( 'NONE',  ( 19.97611676871187569, -6.800378171449690257, -1.500000000000002220 ) ) ;
#20001=CARTESIAN_POINT ( 'NONE',  ( -28.52287095715006870, -23.78714491118143570, -0.6496296804704170258 ) ) ;
#20003=CARTESIAN_POINT ( 'NONE',  ( -115.5228709571500616, -23.48783264082477018, -1.443836473390083475 ) ) ;
#20004=VECTOR ( 'NONE', #70575, 1000.000000000000227 ) ;
#20005=CARTESIAN_POINT ( 'NONE',  ( -68.58953762381672448, -23.48786465467241058, 11.44779295918254647 ) ) ;
#20006=CARTESIAN_POINT ( 'NONE',  ( -39.62287095715005592, -29.50250786944525672, 11.44777988621624232 ) ) ;
#20007=CARTESIAN_POINT ( 'NONE',  ( 14.13103794885040898, -16.47871000921984219, -1.500000000000002220 ) ) ;
#20008=CARTESIAN_POINT ( 'NONE',  ( -86.62287095715004170, -24.64965695001468404, 8.947790433994180503 ) ) ;
#20009=CARTESIAN_POINT ( 'NONE',  ( 1.019757120859956512, 22.21710203930399175, 11.49999999999999645 ) ) ;
#20012=CARTESIAN_POINT ( 'NONE',  ( -92.62287095715005592, -23.47596703998600631, 11.44779298504227860 ) ) ;
#20014=DIRECTION ( 'NONE',  ( 0.000000000000000000, 0.9999999999976377785, 2.173523156925978705E-06 ) ) ;
#20021=DIRECTION ( 'NONE',  ( 0.000000000000000000, -2.173523156925979552E-06, 0.9999999999976378895 ) ) ;
#20022=CARTESIAN_POINT ( 'NONE',  ( -63.52287095715006160, -24.65952944569304606, 1.056160979905695463 ) ) ;
#20023=CARTESIAN_POINT ( 'NONE',  ( -67.62287095715005592, -29.50248528299804818, 1.056150453629036701 ) ) ;
#20025=EDGE_LOOP ( 'NONE', ( #17681, #28841, #33830, #731 ) ) ;
#20026=B_SPLINE_CURVE_WITH_KNOTS ( 'NONE', 3,
 ( #40874, #48501, #65244, #41891 ),
 .UNSPECIFIED., .F., .F.,
 ( 4, 4 ),
 ( 6.358484078632993896E-06, 0.001058107079912193370 ),
 .UNSPECIFIED. ) ;
#20028=CARTESIAN_POINT ( 'NONE',  ( 17.66168439605153395, -8.020940556088177686, 11.49999999999999645 ) ) ;
#20030=CARTESIAN_POINT ( 'NONE',  ( -69.52287095715006160, -23.94994826722564341, -0.6494450866342730277 ) ) ;
#20031=CARTESIAN_POINT ( 'NONE',  ( -6.716530693746936898, -21.44081863256500142, -1.500000000000002220 ) ) ;
#20032=ORIENTED_EDGE ( 'NONE', *, *, #1110, .T. ) ;
#20034=CARTESIAN_POINT ( 'NONE',  ( -45.22287095715006444, -23.47593901973090169, -1.443836447538997758 ) ) ;
#20037=CARTESIAN_POINT ( 'NONE',  ( -130.5728709571500588, -24.47917135695840685, 9.440663514584123561 ) ) ;
#20038=EDGE_CURVE ( 'NONE', #69195, #13115, #17594, .T. ) ;
#20039=CARTESIAN_POINT ( 'NONE',  ( -0.6043519431218743465, -19.59835197619436187, 11.49999999999998934 ) ) ;
#20043=CARTESIAN_POINT ( 'NONE',  ( -14.25192491085926072, -16.12266454619898326, -1.500000000000002220 ) ) ;
#20044=CARTESIAN_POINT ( 'NONE',  ( -121.5895376238167387, -23.48783264082478794, -1.443836473390058384 ) ) ;
#20045=CARTESIAN_POINT ( 'NONE',  ( -81.14580165399679856, -25.31572674173500914, 5.096590159266133568 ) ) ;
#20047=EDGE_CURVE ( 'NONE', #40585, #55689, #88199, .T. ) ;
#20048=DIRECTION ( 'NONE',  ( 0.000000000000000000, 2.173523156893721996E-06, -0.9999999999976377785 ) ) ;
#20049=CARTESIAN_POINT ( 'NONE',  ( -6.529369910325518944, -22.02198592821369516, -1.500000000000002220 ) ) ;
#20051=CARTESIAN_POINT ( 'NONE',  ( -46.62287095715004881, -24.66019654487198665, 8.947790411086135265 ) ) ;
#20052=CARTESIAN_POINT ( 'NONE',  ( -53.50203224161664650, -24.15543982623906771, -0.2315651400026670914 ) ) ;
#20053=CARTESIAN_POINT ( 'NONE',  ( -7.946508460909448956, -18.53024980520100939, 11.49999999999999645 ) ) ;
#20054=CARTESIAN_POINT ( 'NONE',  ( -109.4252266130965552, -25.28814134756654397, 3.135431506998875406 ) ) ;
#20057=CARTESIAN_POINT ( 'NONE',  ( -113.5228709571500758, -23.48783264082477373, -1.443836473390082586 ) ) ;
#20059=CARTESIAN_POINT ( 'NONE',  ( -15.96263503330635380, 11.84234753045382682, -1.500000000000002220 ) ) ;
#20060=CARTESIAN_POINT ( 'NONE',  ( -113.5528542040558051, -24.34968618360933945, 0.1864209137778880254 ) ) ;
#20061=CARTESIAN_POINT ( 'NONE',  ( -19.67082186522023690, -1.387426831159568108, -1.500000000000002220 ) ) ;
#20062=CARTESIAN_POINT ( 'NONE',  ( -126.5902073615529133, -23.96169478059714564, 10.65365249895716637 ) ) ;
#20063=CARTESIAN_POINT ( 'NONE',  ( -125.6228709571501128, -24.62285846362216546, 9.038163152653524435 ) ) ;
#20064=CARTESIAN_POINT ( 'NONE',  ( -79.52287095715006160, -23.47596703998600631, 11.44779298504228571 ) ) ;
#20065=CARTESIAN_POINT ( 'NONE',  ( -9.109090448966927767, 18.51201596650851400, 11.49999999999999645 ) ) ;
#20066=CARTESIAN_POINT ( 'NONE',  ( -39.22484595018107711, -25.27985428963552650, 4.963673027505932644 ) ) ;
#20069=CARTESIAN_POINT ( 'NONE',  ( -21.16080155796574047, 8.166215375980355518, 11.49999999999999645 ) ) ;
#20070=VERTEX_POINT ( 'NONE', #51054 ) ;
#20071=CARTESIAN_POINT ( 'NONE',  ( -29.62287096154833677, -23.39681786206389447, 11.44779298504227860 ) ) ;
#20074=CARTESIAN_POINT ( 'NONE',  ( -63.52208789522248367, -23.48783264082476308, -1.443836473390093245 ) ) ;
#20078=PLANE ( 'NONE',  #54983 ) ;
#20079=CARTESIAN_POINT ( 'NONE',  ( -20.58715743568940226, -9.973749938417524774, -1.500000000000002220 ) ) ;
#20080=FACE_OUTER_BOUND ( 'NONE', #9741, .T. ) ;
#20081=CARTESIAN_POINT ( 'NONE',  ( 15.46703529437019853, -15.08741104398349187, -1.500000000000002220 ) ) ;
#20083=CARTESIAN_POINT ( 'NONE',  ( -50.62287095715005592, -29.50248789122583659, 2.256150453626215580 ) ) ;
#20084=CARTESIAN_POINT ( 'NONE',  ( 22.38532167473930556, -2.757513164441831144, 11.49999999999999645 ) ) ;
#20085=ORIENTED_EDGE ( 'NONE', *, *, #37579, .F. ) ;
#20086=FACE_OUTER_BOUND ( 'NONE', #18424, .T. ) ;
#20087=CARTESIAN_POINT ( 'NONE',  ( 21.52718982488130450, -4.553922534329950089, 11.49999999999998934 ) ) ;
#20088=FACE_OUTER_BOUND ( 'NONE', #18278, .T. ) ;
#20091=ORIENTED_EDGE ( 'NONE', *, *, #54413, .T. ) ;
#20095=CARTESIAN_POINT ( 'NONE',  ( -49.58953762381672448, -23.48786465467241058, 11.44779295918254824 ) ) ;
#20096=EDGE_CURVE ( 'NONE', #100230, #5942, #14302, .T. ) ;
#20100=CARTESIAN_POINT ( 'NONE',  ( -49.28565304951956705, -25.27399216425258643, 6.009773539330731218 ) ) ;
#20101=DIRECTION ( 'NONE',  ( 3.773278334444167608E-23, -1.000000000000000000, 0.000000000000000000 ) ) ;
#20103=CARTESIAN_POINT ( 'NONE',  ( 18.38310620586021571, 8.829655622120887060, -1.500000000000002220 ) ) ;
#20105=ADVANCED_FACE ( 'NONE', ( #83982 ), #28206, .T. ) ;
#20107=PLANE ( 'NONE',  #10465 ) ;
#20108=CARTESIAN_POINT ( 'NONE',  ( -88.62287095715001328, -23.73907113216992215, -1.053371485793224371 ) ) ;
#20109=ADVANCED_FACE ( 'NONE', ( #14461 ), #68270, .T. ) ;
#20110=CARTESIAN_POINT ( 'NONE',  ( -97.52287095715004739, -23.72747288104470087, -1.053458166803225460 ) ) ;
#20111=DIRECTION ( 'NONE',  ( 0.000000000000000000, -0.9999999999976377785, -2.173523156925979975E-06 ) ) ;
#20113=CARTESIAN_POINT ( 'NONE',  ( -29.00221282414159418, -25.21531865948820084, 3.230369517096869370 ) ) ;
#20114=CARTESIAN_POINT ( 'NONE',  ( -33.52287095715006160, -24.65952944569303895, 1.056160979905690134 ) ) ;
#20116=EDGE_CURVE ( 'NONE', #28117, #10751, #88119, .T. ) ;
#20119=CARTESIAN_POINT ( 'NONE',  ( -16.26442346200556344, 12.93145763113255775, -1.500000000000002220 ) ) ;
#20120=VERTEX_POINT ( 'NONE', #22070 ) ;
#20121=CARTESIAN_POINT ( 'NONE',  ( -40.29361789974588959, -25.30535304242862082, 5.078340751659213836 ) ) ;
#20123=CARTESIAN_POINT ( 'NONE',  ( -107.6228709571500701, -29.50250786944525672, 11.44777988621622988 ) ) ;
#20124=CARTESIAN_POINT ( 'NONE',  ( -129.6234738311520971, -24.66019654487200086, 8.947790411086113949 ) ) ;
#20125=VERTEX_POINT ( 'NONE', #83478 ) ;
#20128=CARTESIAN_POINT ( 'NONE',  ( -121.5228709571500048, -23.47593901973090524, -1.443836447538996204 ) ) ;
#20129=CARTESIAN_POINT ( 'NONE',  ( -55.58953762381672448, -23.48783264082478084, -1.443836473390068820 ) ) ;
#20130=CARTESIAN_POINT ( 'NONE',  ( -71.30358265130861639, -25.24515230220021422, 6.178525869656843916 ) ) ;
#20131=CARTESIAN_POINT ( 'NONE',  ( 19.10104996495751450, -11.12853483292915691, 11.49999999999999645 ) ) ;
#20132=EDGE_LOOP ( 'NONE', ( #33237, #80496, #5578, #87474 ) ) ;
#20134=CARTESIAN_POINT ( 'NONE',  ( -15.94491270116497184, -16.04792668696150315, 11.49999999999998934 ) ) ;
#20137=ORIENTED_EDGE ( 'NONE', *, *, #48524, .T. ) ;
#20138=CARTESIAN_POINT ( 'NONE',  ( -78.58953762381672448, -24.66019654487198665, 8.947790411086133489 ) ) ;
#20139=B_SPLINE_CURVE_WITH_KNOTS ( 'NONE', 3,
 ( #43853, #57592, #10905, #73796, #88529, #41868 ),
 .UNSPECIFIED., .F., .F.,
 ( 4, 2, 4 ),
 ( 0.000000000000000000, 0.001380901958385391580, 0.002761803916770783161 ),
 .UNSPECIFIED. ) ;
#20141=CARTESIAN_POINT ( 'NONE',  ( -57.64983551063303224, -23.73791477778911840, 11.05961554403170588 ) ) ;
#20143=CARTESIAN_POINT ( 'NONE',  ( -14.54676392617323266, -15.37779485849079464, 11.49999999999998934 ) ) ;
#20144=CARTESIAN_POINT ( 'NONE',  ( -40.01839366089613748, -25.29345411398207943, 5.509688073139549225 ) ) ;
#20145=CARTESIAN_POINT ( 'NONE',  ( 8.793911523065595759, -20.50603677605392150, -1.500000000000002220 ) ) ;
#20148=CARTESIAN_POINT ( 'NONE',  ( -123.6228709571500559, -24.64898659630368627, 1.056161002820833028 ) ) ;
#20151=CARTESIAN_POINT ( 'NONE',  ( -83.55620429048336462, -24.64965694238574301, 8.947790433994201820 ) ) ;
#20152=CARTESIAN_POINT ( 'NONE',  ( -18.49313839071750820, -6.238557295281221826, 11.49999999999998934 ) ) ;
#20153=CARTESIAN_POINT ( 'NONE',  ( 17.37860173834871347, 12.56526366372364301, -1.500000000000002220 ) ) ;
#20154=CARTESIAN_POINT ( 'NONE',  ( -26.98755670591954114, -24.92774695839280241, 1.764414538584399894 ) ) ;
#20155=CARTESIAN_POINT ( 'NONE',  ( -112.6228709571500559, -29.50247984919015209, -1.443849546365048253 ) ) ;
#20156=CARTESIAN_POINT ( 'NONE',  ( -115.5228709571500616, -24.99132157543084531, 2.256160258750667502 ) ) ;
#20157=ADVANCED_FACE ( 'NONE', ( #20086 ), #28071, .T. ) ;
#20158=CARTESIAN_POINT ( 'NONE',  ( -10.93939140624874007, -20.02795264745160608, -1.500000000000002220 ) ) ;
#20162=CARTESIAN_POINT ( 'NONE',  ( -46.52287095715006160, -24.65952944569304606, 1.056160979905693686 ) ) ;
#20164=CARTESIAN_POINT ( 'NONE',  ( -19.52388446859773552, -3.948942086532154061, 11.49999999999999645 ) ) ;
#20165=CARTESIAN_POINT ( 'NONE',  ( -69.52287095715010423, -23.96127896941631974, -0.6493128931038036900 ) ) ;
#20166=FACE_OUTER_BOUND ( 'NONE', #89490, .T. ) ;
#20167=DIRECTION ( 'NONE',  ( -1.000000000000000000, -3.773278334444166432E-23, -8.201307841325785021E-29 ) ) ;
#20168=ORIENTED_EDGE ( 'NONE', *, *, #66521, .T. ) ;
#20169=CARTESIAN_POINT ( 'NONE',  ( -25.63707821144803845, -24.86039540779550094, 3.655391356329271257 ) ) ;
#20172=CARTESIAN_POINT ( 'NONE',  ( 0.4029737066630413311, -21.70969715354747009, -1.500000000000002220 ) ) ;
#20173=CARTESIAN_POINT ( 'NONE',  ( -88.88918693012689687, -25.25676012837779183, 6.101892527513559372 ) ) ;
#20174=CARTESIAN_POINT ( 'NONE',  ( -19.49195742049215241, -1.735909528584683947, -1.500000000000002220 ) ) ;
#20175=DIRECTION ( 'NONE',  ( 3.773278334444166432E-23, -1.000000000000000000, 0.000000000000000000 ) ) ;
#20176=VERTEX_POINT ( 'NONE', #62663 ) ;
#20179=CARTESIAN_POINT ( 'NONE',  ( -17.38880980700008294, 10.71821138944157603, 11.49999999999999645 ) ) ;
#20180=CARTESIAN_POINT ( 'NONE',  ( -49.28019047777514317, -25.25808854711805651, 6.078199934834979778 ) ) ;
#20181=EDGE_CURVE ( 'NONE', #1269, #56546, #30042, .T. ) ;
#20186=CARTESIAN_POINT ( 'NONE',  ( -116.6298700828398864, -23.48786465467241769, 11.44779295918253759 ) ) ;
#20187=CARTESIAN_POINT ( 'NONE',  ( -109.5906689592580108, -24.15543982623907482, -0.2315651400026587092 ) ) ;
#20188=ORIENTED_EDGE ( 'NONE', *, *, #26083, .F. ) ;
#20190=B_SPLINE_CURVE_WITH_KNOTS ( 'NONE', 3,
 ( #76583, #61394, #92816, #22790 ),
 .UNSPECIFIED., .F., .F.,
 ( 4, 4 ),
 ( 0.4808433584723854071, 0.4898497897445006632 ),
 .UNSPECIFIED. ) ;
#20191=CARTESIAN_POINT ( 'NONE',  ( -21.58539018223340022, -8.019882488244659768, 11.49999999999999645 ) ) ;
#20192=CARTESIAN_POINT ( 'NONE',  ( -21.69093436787670726, -6.948586514802197023, -1.500000000000002220 ) ) ;
#20193=CARTESIAN_POINT ( 'NONE',  ( -70.35039385224574460, -25.31517373849778352, 4.853613849468179531 ) ) ;
#20194=CARTESIAN_POINT ( 'NONE',  ( -110.6228709571500559, -29.50247984919015209, -1.443849546365048253 ) ) ;
#20197=CARTESIAN_POINT ( 'NONE',  ( -70.52287095715009002, -24.63287334234179582, 0.9662140553045422964 ) ) ;
#20199=CARTESIAN_POINT ( 'NONE',  ( 9.607415760296678542, -19.69187540195887465, -1.500000000000002220 ) ) ;
#20200=CARTESIAN_POINT ( 'NONE',  ( -87.55620429048337883, -24.65952944569304606, 1.056160979905701902 ) ) ;
#20204=VERTEX_POINT ( 'NONE', #77849 ) ;
#20205=CARTESIAN_POINT ( 'NONE',  ( -16.87313589883980214, -11.49665204554024989, -1.500000000000002220 ) ) ;
#20206=ORIENTED_EDGE ( 'NONE', *, *, #57500, .F. ) ;
#20207=VERTEX_POINT ( 'NONE', #92091 ) ;
#20209=EDGE_LOOP ( 'NONE', ( #59996, #56442 ) ) ;
#20210=CARTESIAN_POINT ( 'NONE',  ( -1.973530150111237003, 22.95712487800313539, -1.500000000000002220 ) ) ;
#20212=CARTESIAN_POINT ( 'NONE',  ( 18.82617747125253871, -7.458514806974097411, -1.500000000000002220 ) ) ;
#20216=CARTESIAN_POINT ( 'NONE',  ( -48.52287095715006160, -24.66019654487200086, 8.947790411086119278 ) ) ;
#20217=ADVANCED_FACE ( 'NONE', ( #84482 ), #42650, .T. ) ;
#20218=CARTESIAN_POINT ( 'NONE',  ( -95.50969526946468591, -24.40034930558991633, 0.3402023900116099009 ) ) ;
#20219=CARTESIAN_POINT ( 'NONE',  ( -41.62287095715006302, -24.64965695001467694, 8.947790433994187609 ) ) ;
#20220=CARTESIAN_POINT ( 'NONE',  ( 7.684279652734260502, -19.92951104315265809, 11.49999999999999645 ) ) ;
#20221=ORIENTED_EDGE ( 'NONE', *, *, #66082, .T. ) ;
#20223=EDGE_CURVE ( 'NONE', #40883, #35091, #61522, .T. ) ;
#20225=CARTESIAN_POINT ( 'NONE',  ( 14.63995501510512653, -16.76770752772931772, 11.49999999999998934 ) ) ;
#20226=EDGE_CURVE ( 'NONE', #31854, #53293, #42126, .T. ) ;
#20227=CARTESIAN_POINT ( 'NONE',  ( -16.33875328525262560, 12.67428768300982256, -1.500000000000002220 ) ) ;
#20229=ORIENTED_EDGE ( 'NONE', *, *, #4654, .F. ) ;
#20230=CARTESIAN_POINT ( 'NONE',  ( -69.86193069524509269, -25.03707830618030172, 7.590867772707288630 ) ) ;
#20234=CARTESIAN_POINT ( 'NONE',  ( -17.98194200498208062, 10.70670730041394947, -1.500000000000002220 ) ) ;
#20236=CARTESIAN_POINT ( 'NONE',  ( 18.32745805453730981, -11.99952526121574259, 11.49999999999999645 ) ) ;
#20238=CARTESIAN_POINT ( 'NONE',  ( -89.62590178745654157, -24.51419770103157703, 9.386484678747175181 ) ) ;
#20239=CARTESIAN_POINT ( 'NONE',  ( -10.06026007034034464, -20.14757889648583244, -1.500000000000002220 ) ) ;
#20240=CARTESIAN_POINT ( 'NONE',  ( 15.12549221760053086, 14.48511125727034177, -1.500000000000002220 ) ) ;
#20241=DIRECTION ( 'NONE',  ( 1.000000000000000000, 3.773278334444166432E-23, 8.201307841325785021E-29 ) ) ;
#20242=LINE ( 'NONE', #43103, #25383 ) ;
#20246=B_SPLINE_CURVE_WITH_KNOTS ( 'NONE', 3,
 ( #25692, #81486, #79978, #10464, #48553, #49547, #66277, #80477 ),
 .UNSPECIFIED., .F., .F.,
 ( 4, 2, 2, 4 ),
 ( 6.384118678614035137E-06, 0.002007151183507257120, 0.003007534715921580341, 0.004007918248335903127 ),
 .UNSPECIFIED. ) ;
#20247=ORIENTED_EDGE ( 'NONE', *, *, #16028, .F. ) ;
#20248=EDGE_LOOP ( 'NONE', ( #29225, #86890, #22963, #16304 ) ) ;
#20249=PLANE ( 'NONE',  #64491 ) ;
#20250=CARTESIAN_POINT ( 'NONE',  ( -16.43003769262999469, -13.82051474754189258, -1.500000000000002220 ) ) ;
#20251=PLANE ( 'NONE',  #11621 ) ;
#20252=ORIENTED_EDGE ( 'NONE', *, *, #17141, .T. ) ;
#20253=CARTESIAN_POINT ( 'NONE',  ( -17.90976863334866920, 11.11529090135583075, 11.49999999999998934 ) ) ;
#20254=CARTESIAN_POINT ( 'NONE',  ( -36.52287095715006870, -24.65952944569304606, 1.056160979905691910 ) ) ;
#20256=DIRECTION ( 'NONE',  ( -3.773278334444167608E-23, 1.000000000000000000, 0.000000000000000000 ) ) ;
#20258=CARTESIAN_POINT ( 'NONE',  ( -90.62287095715004170, -24.99156045073392818, 7.747789690856161648 ) ) ;
#20259=CARTESIAN_POINT ( 'NONE',  ( -16.97254739485517661, -14.18817111035334655, -1.500000000000002220 ) ) ;
#20260=CARTESIAN_POINT ( 'NONE',  ( -58.62287095715004881, -29.50250786944525672, 11.44777988621623876 ) ) ;
#20262=CARTESIAN_POINT ( 'NONE',  ( -60.57607103537276316, -25.00158670708909980, 2.256160236439220146 ) ) ;
#20266=CARTESIAN_POINT ( 'NONE',  ( 13.34776491790984210, -16.67230741956907991, -1.500000000000002220 ) ) ;
#20267=CARTESIAN_POINT ( 'NONE',  ( -113.5228709571500616, -23.48786465467242479, 11.44779295918253936 ) ) ;
#20268=FACE_BOUND ( 'NONE', #60568, .T. ) ;
#20269=EDGE_CURVE ( 'NONE', #26877, #57581, #74800, .T. ) ;
#20272=CARTESIAN_POINT ( 'NONE',  ( -20.48750165597241590, 9.616757810196778777, -1.500000000000002220 ) ) ;
#20273=ORIENTED_EDGE ( 'NONE', *, *, #51731, .T. ) ;
#20275=CARTESIAN_POINT ( 'NONE',  ( -79.50175546033953822, -24.51314013834316086, 0.6176544820404135105 ) ) ;
#20276=CARTESIAN_POINT ( 'NONE',  ( 19.18382676146983457, -4.683391092530263755, 11.49999999999999645 ) ) ;
#20278=CARTESIAN_POINT ( 'NONE',  ( -67.58378879032223097, -24.51314013834315730, 0.6176544820404126224 ) ) ;
#20280=FACE_OUTER_BOUND ( 'NONE', #11885, .T. ) ;
#20283=CARTESIAN_POINT ( 'NONE',  ( -7.466173891270859286, -20.28576548065916541, 11.49999999999998934 ) ) ;
#20284=CARTESIAN_POINT ( 'NONE',  ( -49.10668015502195516, -25.10935369951826956, 3.950018049247062457 ) ) ;
#20285=CARTESIAN_POINT ( 'NONE',  ( -9.899997732206244905, -16.63842163800745766, -1.500000000000002220 ) ) ;
#20286=CARTESIAN_POINT ( 'NONE',  ( -92.52287095715006160, -23.48783264083452593, -1.443836473374927820 ) ) ;
#20287=CARTESIAN_POINT ( 'NONE',  ( -85.58953762381671027, -25.00182538069145366, 7.747789668545099317 ) ) ;
#20288=CARTESIAN_POINT ( 'NONE',  ( -15.51018552496569392, -12.33189742059753868, 11.49999999999998934 ) ) ;
#20289=ORIENTED_EDGE ( 'NONE', *, *, #22177, .T. ) ;
#20290=B_SPLINE_CURVE_WITH_KNOTS ( 'NONE', 3,
 ( #66802, #97229, #97723, #35338, #5871, #74385 ),
 .UNSPECIFIED., .F., .F.,
 ( 4, 2, 4 ),
 ( 0.000000000000000000, 0.001380764517853252504, 0.002761529035706505007 ),
 .UNSPECIFIED. ) ;
#20291=CARTESIAN_POINT ( 'NONE',  ( -6.888417027594036846, 19.07602104198033643, 11.49999999999999645 ) ) ;
#20292=CARTESIAN_POINT ( 'NONE',  ( -88.52287095715006160, -29.50248528299804818, 1.056150453629040253 ) ) ;
#20297=CARTESIAN_POINT ( 'NONE',  ( -37.52287095715006160, -24.35013146730203815, 9.818937971375104823 ) ) ;
#20300=CARTESIAN_POINT ( 'NONE',  ( -80.52287095715006160, -24.99132157543083821, 2.256160258750667502 ) ) ;
#20301=DIRECTION ( 'NONE',  ( -3.773278334453079030E-23, 0.9999999999976377785, 2.173523156925979128E-06 ) ) ;
#20302=CARTESIAN_POINT ( 'NONE',  ( 20.03642891561555928, 0.6179553080306146029, 11.49999999999998934 ) ) ;
#20308=CARTESIAN_POINT ( 'NONE',  ( -103.5228709571500474, -24.66019654487200441, 8.947790411086119278 ) ) ;
#20309=CARTESIAN_POINT ( 'NONE',  ( -127.5228709571500616, -24.33832256527049154, 0.1851278514138698372 ) ) ;
#20311=FACE_OUTER_BOUND ( 'NONE', #68062, .T. ) ;
#20312=LINE ( 'NONE', #83723, #39705 ) ;
#20314=ORIENTED_EDGE ( 'NONE', *, *, #82552, .F. ) ;
#20315=CARTESIAN_POINT ( 'NONE',  ( -5.305567426876419468, 19.62801697144059787, -1.500000000000002220 ) ) ;
#20318=B_SPLINE_CURVE_WITH_KNOTS ( 'NONE', 3,
 ( #99629, #61107, #69203, #100118 ),
 .UNSPECIFIED., .F., .F.,
 ( 4, 4 ),
 ( 0.4791111652815406852, 0.4801119123223059892 ),
 .UNSPECIFIED. ) ;
#20319=CARTESIAN_POINT ( 'NONE',  ( 20.38051395842347802, -10.57019977742728578, -1.500000000000002220 ) ) ;
#20320=CARTESIAN_POINT ( 'NONE',  ( -32.54531990124663565, -24.15543982623907127, -0.2315651400026567941 ) ) ;
#20321=ORIENTED_EDGE ( 'NONE', *, *, #12141, .F. ) ;
#20322=FACE_OUTER_BOUND ( 'NONE', #85609, .T. ) ;
#20324=CARTESIAN_POINT ( 'NONE',  ( -117.5562042904833930, -23.48786465467241413, 11.44779295918253403 ) ) ;
#20325=CARTESIAN_POINT ( 'NONE',  ( -17.78888362263414535, -11.56919986243916654, 11.49999999999999645 ) ) ;
#20327=AXIS2_PLACEMENT_3D ( 'NONE', #91818, #54779, #99911 ) ;
#20330=CARTESIAN_POINT ( 'NONE',  ( -21.14524153552446606, 6.695245452574716261, 11.49999999999998934 ) ) ;
#20332=CARTESIAN_POINT ( 'NONE',  ( 16.39479758508079144, -12.47777281027006424, -1.500000000000002220 ) ) ;
#20335=CARTESIAN_POINT ( 'NONE',  ( -98.52287095715006160, -29.50250243563736774, 8.947779886222138046 ) ) ;
#20336=FACE_OUTER_BOUND ( 'NONE', #42601, .T. ) ;
#20337=VERTEX_POINT ( 'NONE', #48430 ) ;
#20338=ORIENTED_EDGE ( 'NONE', *, *, #33171, .F. ) ;
#20339=ORIENTED_EDGE ( 'NONE', *, *, #24691, .T. ) ;
#20341=PLANE ( 'NONE',  #4927 ) ;
#20343=CARTESIAN_POINT ( 'NONE',  ( 17.22178217532253086, -11.58000449095910867, -1.500000000000002220 ) ) ;
#20345=CARTESIAN_POINT ( 'NONE',  ( 21.64095104908334122, -2.195182070091274529, 11.49999999999999645 ) ) ;
#20346=ORIENTED_EDGE ( 'NONE', *, *, #77257, .F. ) ;
#20347=CARTESIAN_POINT ( 'NONE',  ( -51.72797971311533161, -25.15689236464227463, 6.906090482414427356 ) ) ;
#20348=CARTESIAN_POINT ( 'NONE',  ( -39.62287095715005592, -23.48786465467240347, 11.44779295918255180 ) ) ;
#20349=CARTESIAN_POINT ( 'NONE',  ( -79.52287095715006160, -29.50250243563736774, 8.947779886222141599 ) ) ;
#20350=CARTESIAN_POINT ( 'NONE',  ( 22.01961411883556252, 4.383451955130949429, -1.500000000000002220 ) ) ;
#20351=CARTESIAN_POINT ( 'NONE',  ( -51.29424904866267099, -25.26334605459731364, 4.063412005954170070 ) ) ;
#20352=CARTESIAN_POINT ( 'NONE',  ( -65.63042981099128781, -24.73486907724918282, 1.287355809206962354 ) ) ;
#20354=LINE ( 'NONE', #11754, #82503 ) ;
#20356=ORIENTED_EDGE ( 'NONE', *, *, #84579, .F. ) ;
#20357=VERTEX_POINT ( 'NONE', #57053 ) ;
#20358=CARTESIAN_POINT ( 'NONE',  ( -87.62287095715004170, -24.64898659630528854, 1.056161002820827921 ) ) ;
#20360=VECTOR ( 'NONE', #76979, 1000.000000000000227 ) ;
#20361=CARTESIAN_POINT ( 'NONE',  ( -19.44786352930952233, -8.617208915446557427, -1.500000000000002220 ) ) ;
#20362=EDGE_LOOP ( 'NONE', ( #24013, #50070, #50373, #85887 ) ) ;
#20363=CARTESIAN_POINT ( 'NONE',  ( -80.62287095715004170, -25.00182538069145721, 7.747789668545097541 ) ) ;
#20364=AXIS2_PLACEMENT_3D ( 'NONE', #98995, #36609, #51346 ) ;
#20365=CARTESIAN_POINT ( 'NONE',  ( 13.86046232669119149, 16.88393516940953276, 11.49999999999998934 ) ) ;
#20366=CARTESIAN_POINT ( 'NONE',  ( -45.58953762381671737, -23.48783264082478084, -1.443836473390070374 ) ) ;
#20367=CARTESIAN_POINT ( 'NONE',  ( 21.55457256799317278, 7.124301260279622738, 11.49999999999998934 ) ) ;
#20368=CARTESIAN_POINT ( 'NONE',  ( -112.5228709571500616, -24.65952944569304961, 1.056160979905704123 ) ) ;
#20370=CARTESIAN_POINT ( 'NONE',  ( -49.52287095715006160, -23.48786465467241769, 11.44779295918255002 ) ) ;
#20371=CARTESIAN_POINT ( 'NONE',  ( 21.10488023177059347, -6.046698511884514460, -1.500000000000002220 ) ) ;
#20372=CARTESIAN_POINT ( 'NONE',  ( -109.5228709571500332, -24.35013146730204525, 9.818937971375099494 ) ) ;
#20374=CARTESIAN_POINT ( 'NONE',  ( -122.5207639614473578, -23.96169478059714564, 10.65365249895717170 ) ) ;
#20379=CARTESIAN_POINT ( 'NONE',  ( -90.62287095715002749, -24.63287334234179582, 0.9662140553045412972 ) ) ;
#20380=CARTESIAN_POINT ( 'NONE',  ( -128.6228709571500417, -23.47596703998600631, 11.44779298504227860 ) ) ;
#20382=CARTESIAN_POINT ( 'NONE',  ( -19.37389216307569129, 8.798533688548827669, 11.49999999999998934 ) ) ;
#20383=CARTESIAN_POINT ( 'NONE',  ( -55.62287095715004170, -25.00182538069145011, 7.747789668545097541 ) ) ;
#20384=CARTESIAN_POINT ( 'NONE',  ( -26.17837527425876942, -24.97064757944748337, 3.912474131936358734 ) ) ;
#20385=CARTESIAN_POINT ( 'NONE',  ( -85.62363011676973201, -25.00158670708910691, 2.256160236439219258 ) ) ;
#20386=CARTESIAN_POINT ( 'NONE',  ( -109.2228709571500787, -23.47596703998600631, 11.44779298504227860 ) ) ;
#20389=ORIENTED_EDGE ( 'NONE', *, *, #33412, .F. ) ;
#20390=CARTESIAN_POINT ( 'NONE',  ( 10.86043079284791091, -16.25897383129715834, 11.49999999999999645 ) ) ;
#20391=CARTESIAN_POINT ( 'NONE',  ( -108.5228709571500616, -24.50321055353804311, 9.387540953477509831 ) ) ;
#20392=CARTESIAN_POINT ( 'NONE',  ( -29.80788156245805354, -25.24357952813885575, 5.313887825940373233 ) ) ;
#20395=CARTESIAN_POINT ( 'NONE',  ( -40.55620429048339304, -23.47596703998600276, 11.44779298504227505 ) ) ;
#20396=CARTESIAN_POINT ( 'NONE',  ( -31.62287095715005236, -24.64898659630367206, 1.056161002820817485 ) ) ;
#20397=DIRECTION ( 'NONE',  ( -3.773278334453079030E-23, 0.9999999999976377785, 2.173523156925979128E-06 ) ) ;
#20398=CARTESIAN_POINT ( 'NONE',  ( 19.47230031930329730, 2.946587627359682493, 11.49999999999998934 ) ) ;
#20400=LINE ( 'NONE', #89439, #60218 ) ;
#20405=CARTESIAN_POINT ( 'NONE',  ( -107.5228709571500758, -24.64965694238575011, 8.947790433994192938 ) ) ;
#20407=CARTESIAN_POINT ( 'NONE',  ( -47.54067575102843080, -24.34968618360933590, 0.1864209137778879144 ) ) ;
#20408=CARTESIAN_POINT ( 'NONE',  ( -118.5933790690151142, -23.48783264082477018, -1.443836473390085695 ) ) ;
#20410=ADVANCED_FACE ( 'NONE', ( #65176 ), #40134, .T. ) ;
#20411=B_SPLINE_CURVE_WITH_KNOTS ( 'NONE', 3,
 ( #69882, #16087, #873, #15583, #77969, #16581 ),
 .UNSPECIFIED., .F., .F.,
 ( 4, 2, 4 ),
 ( 0.000000000000000000, 0.001380901958385385509, 0.002761803916770771018 ),
 .UNSPECIFIED. ) ;
#20412=CARTESIAN_POINT ( 'NONE',  ( -69.57050707393172218, -25.24515113043987569, 5.639419424395426539 ) ) ;
#20414=CARTESIAN_POINT ( 'NONE',  ( 19.20567810191101898, 5.375360269454119155, -1.500000000000002220 ) ) ;
#20415=CARTESIAN_POINT ( 'NONE',  ( -32.52287095715008292, -24.33832256527048088, 0.1851278514138551823 ) ) ;
#20416=CARTESIAN_POINT ( 'NONE',  ( -0.1188546349483167036, -21.51133334980950806, -1.019432251695407299 ) ) ;
#20418=EDGE_CURVE ( 'NONE', #32572, #72422, #62797, .T. ) ;
#20419=LINE ( 'NONE', #66646, #2201 ) ;
#20421=EDGE_CURVE ( 'NONE', #58389, #36250, #5734, .T. ) ;
#20426=CARTESIAN_POINT ( 'NONE',  ( -124.4728709572981131, -25.30561156594276184, 5.197832205049725651 ) ) ;
#20427=CARTESIAN_POINT ( 'NONE',  ( -81.62638369177169295, -24.51314013834316796, 0.6176544820404249458 ) ) ;
#20428=B_SPLINE_CURVE_WITH_KNOTS ( 'NONE', 3,
 ( #31742, #25117, #63209, #79409 ),
 .UNSPECIFIED., .F., .F.,
 ( 4, 4 ),
 ( 0.7803431484189624623, 0.7893495796910778850 ),
 .UNSPECIFIED. ) ;
#20432=ORIENTED_EDGE ( 'NONE', *, *, #46057, .T. ) ;
#20436=ORIENTED_EDGE ( 'NONE', *, *, #97893, .F. ) ;
#20438=CARTESIAN_POINT ( 'NONE',  ( 18.19722386731275066, -8.884848157732822216, 11.49999999999998934 ) ) ;
#20440=CARTESIAN_POINT ( 'NONE',  ( -105.5228709571500616, -24.99156044556202971, 7.747789690856173195 ) ) ;
#20441=VECTOR ( 'NONE', #82686, 1000.000000000000114 ) ;
#20442=CARTESIAN_POINT ( 'NONE',  ( -43.62287095715004881, -24.64898659630367206, 1.056161002820819261 ) ) ;
#20443=B_SPLINE_CURVE_WITH_KNOTS ( 'NONE', 3,
 ( #99161, #51514, #29659, #74831, #61126, #22525 ),
 .UNSPECIFIED., .F., .F.,
 ( 4, 2, 4 ),
 ( 6.384118678613478637E-06, 0.001386860460828377587, 0.002767336802978141459 ),
 .UNSPECIFIED. ) ;
#20444=AXIS2_PLACEMENT_3D ( 'NONE', #46409, #31175, #23047 ) ;
#20445=CARTESIAN_POINT ( 'NONE',  ( -76.62287095715007013, -24.51283580621364422, 0.6167428607019831421 ) ) ;
#20447=CARTESIAN_POINT ( 'NONE',  ( -79.89320743519122914, -25.31550070763928773, 5.063404179320856180 ) ) ;
#20449=CARTESIAN_POINT ( 'NONE',  ( 15.84714387567644955, -12.28532832577633194, -1.500000000000002220 ) ) ;
#20450=CARTESIAN_POINT ( 'NONE',  ( 17.02745815656931683, -12.38318283856952107, 11.49999999999999645 ) ) ;
#20451=LINE ( 'NONE', #89480, #8051 ) ;
#20452=CARTESIAN_POINT ( 'NONE',  ( -111.6228709571500559, -23.72773821059536559, 11.05748984161097326 ) ) ;
#20453=CARTESIAN_POINT ( 'NONE',  ( -21.12782282263547984, 6.412464199276892707, 11.49999999999998934 ) ) ;
#20455=CARTESIAN_POINT ( 'NONE',  ( -96.52287095715004739, -24.33832256527049154, 0.1851278514138652020 ) ) ;
#20456=CARTESIAN_POINT ( 'NONE',  ( -47.62287095715005592, -24.33832256527047733, 0.1851278514138583187 ) ) ;
#20457=CARTESIAN_POINT ( 'NONE',  ( -50.20044999871004165, -25.27344762162802994, 3.305837191087945381 ) ) ;
#20458=ORIENTED_EDGE ( 'NONE', *, *, #79093, .F. ) ;
#20459=EDGE_CURVE ( 'NONE', #5012, #24383, #65131, .T. ) ;
#20460=LINE ( 'NONE', #90483, #26776 ) ;
#20461=CARTESIAN_POINT ( 'NONE',  ( -31.65921402591105505, -23.73766607897669800, -1.055555164236445131 ) ) ;
#20462=ORIENTED_EDGE ( 'NONE', *, *, #14668, .T. ) ;
#20463=ORIENTED_EDGE ( 'NONE', *, *, #98132, .F. ) ;
#20464=CARTESIAN_POINT ( 'NONE',  ( -41.52287095715006870, -23.48786465467240347, 11.44779295918255180 ) ) ;
#20467=CARTESIAN_POINT ( 'NONE',  ( -11.86786554430972096, -16.85652113839894639, -1.500000000000002220 ) ) ;
#20468=EDGE_CURVE ( 'NONE', #55380, #88518, #16645, .T. ) ;
#20469=CARTESIAN_POINT ( 'NONE',  ( -20.99440926880444636, 4.982473936180791263, 11.49999999999999645 ) ) ;
#20471=CARTESIAN_POINT ( 'NONE',  ( -49.86436991692592358, -25.15008860783680333, 7.002718424707902400 ) ) ;
#20472=CARTESIAN_POINT ( 'NONE',  ( -105.6228709571500559, -23.47596703998600631, 11.44779298504227860 ) ) ;
#20473=VECTOR ( 'NONE', #96044, 1000.000000000000114 ) ;
#20475=CARTESIAN_POINT ( 'NONE',  ( 22.34790896907852442, -0.4833156648990815651, 11.49999999999998934 ) ) ;
#20476=EDGE_CURVE ( 'NONE', #24634, #81045, #14831, .T. ) ;
#20477=CARTESIAN_POINT ( 'NONE',  ( -100.4426124108961176, -25.13313949306887451, 7.101635536975466678 ) ) ;
#20479=EDGE_LOOP ( 'NONE', ( #21722, #40701, #20188, #70244 ) ) ;
#20480=EDGE_CURVE ( 'NONE', #5271, #20866, #79655, .T. ) ;
#20483=CARTESIAN_POINT ( 'NONE',  ( 14.99592430652175956, 14.54719766626331889, 11.49999999999998934 ) ) ;
#20484=ORIENTED_EDGE ( 'NONE', *, *, #20727, .T. ) ;
#20485=CARTESIAN_POINT ( 'NONE',  ( -90.62287095715004170, -29.50249982740957577, 7.747779886224967605 ) ) ;
#20486=ORIENTED_EDGE ( 'NONE', *, *, #86723, .F. ) ;
#20488=CARTESIAN_POINT ( 'NONE',  ( -51.29687923781917647, -25.26364009307625125, 3.993462176398971497 ) ) ;
#20489=CARTESIAN_POINT ( 'NONE',  ( -15.55823947972799282, -14.28038451723262270, -1.500000000000002220 ) ) ;
#20490=EDGE_LOOP ( 'NONE', ( #2413, #71673, #57730, #84408, #89612, #11776, #40595, #96022, #5634, #15227, #24813, #7012, #76851, #62443, #27991, #64727, #99740, #44982, #90818, #32072, #24633, #21724, #57801, #78598, #85526, #86689, #10018, #94199, #32882, #34266, #44697, #76486, #28074, #30508, #28330, #79393, #42077, #33827, #95917, #62756, #84768, #81809, #69292, #31965, #98704, #4181, #80121, #22968, #12152, #4604, #90735, #73260, #55842, #36225, #43278, #15828, #50968, #48616, #23199, #22468, #72409, #15719, #42537, #2178, #60718, #39440, #95360, #87129, #37073, #35811, #62699, #47090, #15870, #30720, #57817, #55931, #8846, #37482, #52331, #53986, #60962, #9908, #10511, #52055, #26876, #75203, #92337, #18733, #90533, #54837, #74773, #751, #3417, #29234, #89618, #79266, #69761, #42560, #58477, #96710, #5035, #26940, #78086, #73221, #20596, #15841, #16756, #50997, #64907, #4962, #39573, #32118, #76634, #67415, #98027, #56956, #88065, #36440, #78962, #50964, #99906, #18477, #72074, #31204, #26565, #1103, #52211, #4771, #22080, #43207, #83971, #27696, #9491, #53507, #53701, #96761, #56059, #75465, #64321, #42615, #5466, #12489, #6627, #66549, #55203, #6257, #4892, #33376, #83610, #80647, #44862, #11860, #45873, #52934, #83540, #17732, #35757, #68961, #10893, #53721, #87754, #61294, #28285, #26003, #61808, #78829, #50336, #55427, #48495, #31442, #85396, #19724, #42494, #13089, #37570, #5068, #25707, #29122, #37964, #50900, #71175, #35969, #62832, #76392, #85358, #53081, #18031, #25013, #59410, #83224, #31239, #80202, #6122, #92017, #71984, #83535, #8152, #87281, #58434, #81121, #3332, #33196 ) ) ;
#20491=CARTESIAN_POINT ( 'NONE',  ( -128.5228709571500758, -24.65952944569305316, 1.056160979905707675 ) ) ;
#20493=FACE_OUTER_BOUND ( 'NONE', #14222, .T. ) ;
#20495=PLANE ( 'NONE',  #31937 ) ;
#20496=CARTESIAN_POINT ( 'NONE',  ( -21.72135255055207281, 0.4632500610043824851, -1.500000000000002220 ) ) ;
#20497=CARTESIAN_POINT ( 'NONE',  ( -81.22562555205841761, -25.12224328816577312, 6.810745100948484065 ) ) ;
#20498=CARTESIAN_POINT ( 'NONE',  ( -11.77839732991513166, 18.97803183815481987, 11.49999999999999645 ) ) ;
#20500=CARTESIAN_POINT ( 'NONE',  ( -42.52287095715004739, -23.48783264083366973, -1.443836473376261642 ) ) ;
#20502=CARTESIAN_POINT ( 'NONE',  ( -106.5228709571500900, -23.72773821059536914, 11.05748984161097326 ) ) ;
#20503=VERTEX_POINT ( 'NONE', #33451 ) ;
#20507=CARTESIAN_POINT ( 'NONE',  ( -100.5101156622768031, -25.13331755552596647, 7.100618926951157484 ) ) ;
#20510=CARTESIAN_POINT ( 'NONE',  ( -67.52287095715006160, -23.47596703998600631, 11.44779298504228748 ) ) ;
#20513=CARTESIAN_POINT ( 'NONE',  ( -31.52287095715006160, -23.48786465467240347, 11.44779295918255357 ) ) ;
#20514=VERTEX_POINT ( 'NONE', #45798 ) ;
#20516=CARTESIAN_POINT ( 'NONE',  ( -4.359330469889163950, 18.88329184224734192, 11.49999999999999645 ) ) ;
#20517=CARTESIAN_POINT ( 'NONE',  ( -81.58953762381673869, -23.47596703998600276, 11.44779298504227683 ) ) ;
#20519=ORIENTED_EDGE ( 'NONE', *, *, #91117, .F. ) ;
#20522=CARTESIAN_POINT ( 'NONE',  ( -122.5228709571500616, -23.48786465467241769, 11.44779295918253759 ) ) ;
#20524=CARTESIAN_POINT ( 'NONE',  ( -36.52287095715006870, -23.73934037231755667, 11.05740245334329153 ) ) ;
#20525=CARTESIAN_POINT ( 'NONE',  ( 14.99095386781537975, 12.61000069877385421, 11.49999999999998934 ) ) ;
#20528=CARTESIAN_POINT ( 'NONE',  ( 19.31049906410359895, -9.575588319827552652, -1.500000000000002220 ) ) ;
#20529=CARTESIAN_POINT ( 'NONE',  ( -56.55620429048340014, -24.64898659630528499, 1.056161002820820594 ) ) ;
#20530=CARTESIAN_POINT ( 'NONE',  ( -70.61198345729647485, -25.25639593825978579, 7.066381960558362429 ) ) ;
#20531=LINE ( 'NONE', #5316, #3872 ) ;
#20532=B_SPLINE_CURVE_WITH_KNOTS ( 'NONE', 3,
 ( #91072, #22047, #36797, #29173 ),
 .UNSPECIFIED., .F., .F.,
 ( 4, 4 ),
 ( 0.000000000000000000, 0.0001000000000000028644 ),
 .UNSPECIFIED. ) ;
#20533=CARTESIAN_POINT ( 'NONE',  ( -99.72418814851606328, -25.27473278399916623, 3.555267675504576008 ) ) ;
#20534=CARTESIAN_POINT ( 'NONE',  ( -19.06187107478486098, -12.82570580458313003, -1.500000000000002220 ) ) ;
#20535=EDGE_CURVE ( 'NONE', #79071, #100041, #38168, .T. ) ;
#20537=CARTESIAN_POINT ( 'NONE',  ( -101.3738023147422780, -25.27307239909452008, 3.986250617436227550 ) ) ;
#20538=LINE ( 'NONE', #22025, #32878 ) ;
#20539=CARTESIAN_POINT ( 'NONE',  ( -6.497366621441947210, -19.08602653180391329, 11.49999999999999645 ) ) ;
#20545=CARTESIAN_POINT ( 'NONE',  ( 3.337697395173636394, -19.57427954046807983, 11.49999999999998934 ) ) ;
#20546=CARTESIAN_POINT ( 'NONE',  ( -47.58953762381672448, -24.66019654487199020, 8.947790411086131712 ) ) ;
#20548=CARTESIAN_POINT ( 'NONE',  ( 19.26447527235507451, 4.322997736827044690, -1.500000000000002220 ) ) ;
#20549=VECTOR ( 'NONE', #95496, 1000.000000000000114 ) ;
#20550=EDGE_CURVE ( 'NONE', #1418, #23841, #75943, .T. ) ;
#20551=CARTESIAN_POINT ( 'NONE',  ( -126.5555559438642490, -24.15620529776629155, 10.23563542870658871 ) ) ;
#20553=B_SPLINE_CURVE_WITH_KNOTS ( 'NONE', 3,
 ( #69332, #62745, #30770, #55120 ),
 .UNSPECIFIED., .F., .F.,
 ( 4, 4 ),
 ( 0.000000000000000000, 0.0001000000000000028644 ),
 .UNSPECIFIED. ) ;
#20555=EDGE_CURVE ( 'NONE', #53154, #57700, #94212, .T. ) ;
#20558=CARTESIAN_POINT ( 'NONE',  ( 13.32396043830641830, 15.83023408377254704, 11.49999999999999645 ) ) ;
#20560=DIRECTION ( 'NONE',  ( -3.773278334453079618E-23, 0.9999999999976377785, 2.173523156925979975E-06 ) ) ;
#20562=CARTESIAN_POINT ( 'NONE',  ( -14.80616194778269623, -17.16973004002414882, 11.49999999999999645 ) ) ;
#20566=EDGE_CURVE ( 'NONE', #88518, #18541, #21603, .T. ) ;
#20567=CARTESIAN_POINT ( 'NONE',  ( -63.63676973242693435, -24.15543982623906771, -0.2315651400026651485 ) ) ;
#20572=EDGE_CURVE ( 'NONE', #4586, #47607, #99558, .T. ) ;
#20573=DIRECTION ( 'NONE',  ( 0.000000000000000000, 0.9999999999976377785, 2.173523156925979128E-06 ) ) ;
#20574=CARTESIAN_POINT ( 'NONE',  ( -22.23020047961643186, 5.420056861400933457, -1.500000000000002220 ) ) ;
#20575=CARTESIAN_POINT ( 'NONE',  ( -29.59428796461985911, -24.07610702673311209, -0.2315648265717072385 ) ) ;
#20576=CARTESIAN_POINT ( 'NONE',  ( 20.98369277809155165, -4.918611649023987731, -1.500000000000002220 ) ) ;
#20577=CARTESIAN_POINT ( 'NONE',  ( -113.5569086508091488, -23.73791477778911840, 11.05961554403170233 ) ) ;
#20578=CARTESIAN_POINT ( 'NONE',  ( -115.5895376238167245, -24.99156044556120904, 7.747789690856344613 ) ) ;
#20579=CARTESIAN_POINT ( 'NONE',  ( 6.619388286264371146, -21.57091762011834390, 11.49999999999999645 ) ) ;
#20582=CARTESIAN_POINT ( 'NONE',  ( 14.26656746985186608, 16.74056184347216458, -1.500000000000002220 ) ) ;
#20583=EDGE_CURVE ( 'NONE', #56064, #67264, #11914, .T. ) ;
#20585=CARTESIAN_POINT ( 'NONE',  ( -111.5879375875708917, -24.51314013834316796, 0.6176544820404210601 ) ) ;
#20586=CARTESIAN_POINT ( 'NONE',  ( -28.45645220296530908, -25.21724939687763367, 7.353599707584590917 ) ) ;
#20589=CARTESIAN_POINT ( 'NONE',  ( -90.58192276783553609, -25.00182538069147142, 7.747789668545044250 ) ) ;
#20590=EDGE_LOOP ( 'NONE', ( #72998, #91486, #91084, #77620 ) ) ;
#20594=AXIS2_PLACEMENT_3D ( 'NONE', #36111, #67080, #44232 ) ;
#20595=B_SPLINE_CURVE_WITH_KNOTS ( 'NONE', 3,
 ( #32213, #78380, #39830, #16989, #94112, #24598 ),
 .UNSPECIFIED., .F., .F.,
 ( 4, 2, 4 ),
 ( 0.000000000000000000, 0.001380764517854769086, 0.002761529035709538171 ),
 .UNSPECIFIED. ) ;
#20596=ORIENTED_EDGE ( 'NONE', *, *, #13147, .F. ) ;
#20597=CARTESIAN_POINT ( 'NONE',  ( -61.52287095715006160, -29.50250786944525672, 11.44777988621623876 ) ) ;
#20599=CARTESIAN_POINT ( 'NONE',  ( -102.6228709571500559, -23.47593901973091235, -1.443836447539001089 ) ) ;
#20600=CARTESIAN_POINT ( 'NONE',  ( 9.511415417357532931, -18.05363124325620205, -1.500000000000002220 ) ) ;
#20601=ORIENTED_EDGE ( 'NONE', *, *, #47186, .F. ) ;
#20603=CARTESIAN_POINT ( 'NONE',  ( -99.52287095715000476, -23.73934037231757443, 11.05740245334328442 ) ) ;
#20604=EDGE_CURVE ( 'NONE', #73483, #26090, #10116, .T. ) ;
#20605=CARTESIAN_POINT ( 'NONE',  ( -105.5081720153104357, -24.92564183028979130, 1.928384488918251316 ) ) ;
#20606=CARTESIAN_POINT ( 'NONE',  ( -70.40598983096596442, -25.25855381519730258, 7.561208889967863556 ) ) ;
#20607=ORIENTED_EDGE ( 'NONE', *, *, #9217, .T. ) ;
#20611=CARTESIAN_POINT ( 'NONE',  ( -6.767879454864726974, -19.68250801024624508, -1.500000000000002220 ) ) ;
#20614=PLANE ( 'NONE',  #47467 ) ;
#20615=ORIENTED_EDGE ( 'NONE', *, *, #83229, .F. ) ;
#20616=CARTESIAN_POINT ( 'NONE',  ( -91.94687923781918926, -25.23397913219354649, 6.409327625488847602 ) ) ;
#20617=CARTESIAN_POINT ( 'NONE',  ( -56.58953762381675290, -23.47596703998600276, 11.44779298504227505 ) ) ;
#20620=CARTESIAN_POINT ( 'NONE',  ( -33.52287095715008292, -24.33927499327854349, 9.819080762295817166 ) ) ;
#20622=CARTESIAN_POINT ( 'NONE',  ( -119.4336594584714391, -25.30053190447140921, 4.607786779764230012 ) ) ;
#20623=CARTESIAN_POINT ( 'NONE',  ( -52.62287095715006302, -24.35013146730203815, 9.818937971375113705 ) ) ;
#20624=CARTESIAN_POINT ( 'NONE',  ( -71.04293837957820301, -25.31201647013682887, 5.573254820805182419 ) ) ;
#20625=CARTESIAN_POINT ( 'NONE',  ( 13.35222405703702186, 17.66689192352044913, 11.49999999999999645 ) ) ;
#20626=ORIENTED_EDGE ( 'NONE', *, *, #97578, .T. ) ;
#20627=CARTESIAN_POINT ( 'NONE',  ( -108.6278311533503143, -24.15543982623907837, -0.2315651400026445539 ) ) ;
#20628=CARTESIAN_POINT ( 'NONE',  ( -11.86362535333686807, -19.25999739251378173, -1.500000000000002220 ) ) ;
#20629=AXIS2_PLACEMENT_3D ( 'NONE', #12262, #27513, #43241 ) ;
#20630=CARTESIAN_POINT ( 'NONE',  ( -115.5183015014103916, -24.15602025860897584, 10.28564288303533836 ) ) ;
#20631=ORIENTED_EDGE ( 'NONE', *, *, #25606, .F. ) ;
#20632=B_SPLINE_CURVE_WITH_KNOTS ( 'NONE', 3,
 ( #18776, #64993, #79178, #86791, #88306, #65492 ),
 .UNSPECIFIED., .F., .F.,
 ( 4, 2, 4 ),
 ( 0.000000000000000000, 0.001380764517854764098, 0.002761529035709528197 ),
 .UNSPECIFIED. ) ;
#20635=CARTESIAN_POINT ( 'NONE',  ( -127.6228709571500559, -23.48783264082479505, -1.443836473390056829 ) ) ;
#20636=CARTESIAN_POINT ( 'NONE',  ( -89.40841769935769889, -25.23397913219577049, 6.409327625469732226 ) ) ;
#20637=VERTEX_POINT ( 'NONE', #9115 ) ;
#20638=CARTESIAN_POINT ( 'NONE',  ( -126.5228709571499763, -23.48783264082477018, -1.443836473390082142 ) ) ;
#20639=CARTESIAN_POINT ( 'NONE',  ( 7.190675130926929448, -21.12231643677837312, -1.500000000000002220 ) ) ;
#20641=VERTEX_POINT ( 'NONE', #78607 ) ;
#20642=CARTESIAN_POINT ( 'NONE',  ( -115.5228709571500616, -29.50249982740957577, 7.747779886224967605 ) ) ;
#20644=CARTESIAN_POINT ( 'NONE',  ( -27.70544111104076990, -24.60484793945295934, 1.628749883096155981 ) ) ;
#20646=CARTESIAN_POINT ( 'NONE',  ( -49.62287095715007013, -24.33927499327854704, 9.819080762295820719 ) ) ;
#20648=CARTESIAN_POINT ( 'NONE',  ( -13.24781383850973349, 14.34467480260970795, 11.49999999999998934 ) ) ;
#20649=CARTESIAN_POINT ( 'NONE',  ( -20.86232423683148340, -5.086641213604358391, 11.49999999999998934 ) ) ;
#20650=CARTESIAN_POINT ( 'NONE',  ( -27.12458168156152638, -24.92774685199402285, 1.715462320597556323 ) ) ;
#20651=CARTESIAN_POINT ( 'NONE',  ( -83.62287095715005592, -23.47593901973091235, -1.443836447539004642 ) ) ;
#20652=CARTESIAN_POINT ( 'NONE',  ( -120.5562042904833930, -24.99156044556202616, 7.747789690856173195 ) ) ;
#20653=CARTESIAN_POINT ( 'NONE',  ( -2.521034868938843765, 22.70145277337256218, -1.500000000000002220 ) ) ;
#20654=VECTOR ( 'NONE', #53191, 1000.000000000000114 ) ;
#20658=CARTESIAN_POINT ( 'NONE',  ( 19.86680303116296287, 2.261939200664708327, 11.49999999999999645 ) ) ;
#20663=CARTESIAN_POINT ( 'NONE',  ( -39.56974522548517825, -23.48786465467240347, 11.44779295918255002 ) ) ;
#20664=CARTESIAN_POINT ( 'NONE',  ( -101.6228709571500559, -24.50216790748099882, 0.6166512839513650368 ) ) ;
#20665=VERTEX_POINT ( 'NONE', #48701 ) ;
#20669=CARTESIAN_POINT ( 'NONE',  ( 21.03555826204448209, -5.341079136732027166, -1.500000000000002220 ) ) ;
#20671=CARTESIAN_POINT ( 'NONE',  ( 9.052818235119415746, 17.31195010612007223, -1.500000000000002220 ) ) ;
#20672=EDGE_CURVE ( 'NONE', #83541, #99862, #51811, .T. ) ;
#20673=CARTESIAN_POINT ( 'NONE',  ( -128.6228709571500417, -29.50247984919015209, -1.443849546365044922 ) ) ;
#20676=CARTESIAN_POINT ( 'NONE',  ( -47.52287095715006160, -29.50250243563736774, 8.947779886222146928 ) ) ;
#20678=CARTESIAN_POINT ( 'NONE',  ( -19.72667040167412722, -5.651925516699977337, 11.49999999999999645 ) ) ;
#20679=CARTESIAN_POINT ( 'NONE',  ( -49.31826291143544694, -25.27387648715609458, 5.882378102033829492 ) ) ;
#20680=CARTESIAN_POINT ( 'NONE',  ( -113.5895376238167245, -24.66019654487199730, 8.947790411086124607 ) ) ;
#20684=CARTESIAN_POINT ( 'NONE',  ( -43.58953762381672448, -24.66019654487199375, 8.947790411086137041 ) ) ;
#20685=CARTESIAN_POINT ( 'NONE',  ( -78.62287095715008434, -24.50216790748098816, 0.6166512839513725863 ) ) ;
#20686=CARTESIAN_POINT ( 'NONE',  ( -61.62287095715004881, -23.47593901973091235, -1.443836447539007972 ) ) ;
#20690=CARTESIAN_POINT ( 'NONE',  ( -18.50152239663938403, 13.63810111590111163, 11.49999999999999645 ) ) ;
#20691=CARTESIAN_POINT ( 'NONE',  ( -21.15473383059569557, 8.456223909384457116, -1.500000000000002220 ) ) ;
#20693=B_SPLINE_SURFACE_WITH_KNOTS ( 'NONE', 3, 3, ( 
 ( #44214, #13240, #20852, #51828 ),
 ( #96490, #75147, #43710, #81768 ),
 ( #66073, #35104, #35605, #5637 ),
 ( #21346, #36094, #57953, #82264 ),
 ( #82758, #67063, #12238, #97971 ),
 ( #98474, #26982, #89879, #67555 ),
 ( #36583, #11749, #51322, #13738 ),
 ( #52323, #44709, #42727, #4152 ),
 ( #28471, #58448, #59436, #90377 ),
 ( #83258, #28972, #3658, #88891 ) ),
 .UNSPECIFIED., .F., .F., .F.,
 ( 4, 3, 3, 4 ),
 ( 4, 4 ),
 ( 0.0004766839783822019588, 0.1491231665100172521, 0.2234464077758347988, 0.2977696490416523178 ),
 ( 0.1495120545021637604, 0.1506138731775905903 ),
 .UNSPECIFIED. ) ;
#20695=CARTESIAN_POINT ( 'NONE',  ( -120.5228709571500900, -24.51254535375842636, 9.355368624242261788 ) ) ;
#20696=CARTESIAN_POINT ( 'NONE',  ( -115.5228709571500758, -24.83602698348160231, 1.605859176311261960 ) ) ;
#20697=CARTESIAN_POINT ( 'NONE',  ( -110.6241304692883034, -24.92564183028978775, 1.928384488918251982 ) ) ;
#20698=CARTESIAN_POINT ( 'NONE',  ( 20.57945552106664877, -7.502658216658728563, -1.500000000000002220 ) ) ;
#20701=CARTESIAN_POINT ( 'NONE',  ( -112.6228709571500843, -24.50216790748099527, 0.6166512839513660360 ) ) ;
#20702=CARTESIAN_POINT ( 'NONE',  ( -58.53403895608763463, -24.65952944569304606, 1.056160979905697461 ) ) ;
#20704=PRODUCT ( 'Measuring Tape_Varsay\X2\0131\X0\lan', 'Measuring Tape_Varsay\X2\0131\X0\lan', '', ( #23519 ) ) ;
#20705=CARTESIAN_POINT ( 'NONE',  ( 9.418145840992488971, -18.15903486995133065, 11.49999999999998934 ) ) ;
#20707=ORIENTED_EDGE ( 'NONE', *, *, #5704, .T. ) ;
#20708=ORIENTED_EDGE ( 'NONE', *, *, #85849, .T. ) ;
#20709=EDGE_LOOP ( 'NONE', ( #72221, #97837, #44228, #22161 ) ) ;
#20710=CARTESIAN_POINT ( 'NONE',  ( 11.60186680256600233, 19.91347440808847935, -1.500000000000002220 ) ) ;
#20711=CARTESIAN_POINT ( 'NONE',  ( -61.59282253940321539, -24.15543982623907127, -0.2315651400026656481 ) ) ;
#20712=B_SPLINE_CURVE_WITH_KNOTS ( 'NONE', 3,
 ( #68862, #7450, #84576, #85577, #22167, #99780 ),
 .UNSPECIFIED., .F., .F.,
 ( 4, 2, 4 ),
 ( 0.000000000000000000, 0.001380764517854764966, 0.002761529035709529931 ),
 .UNSPECIFIED. ) ;
#20713=CARTESIAN_POINT ( 'NONE',  ( 2.165584020960389822, 20.11889322763239107, -1.500000000000002220 ) ) ;
#20714=ORIENTED_EDGE ( 'NONE', *, *, #58488, .F. ) ;
#20715=CARTESIAN_POINT ( 'NONE',  ( -97.62287095715004170, -23.96127896941632685, -0.6493128931037805973 ) ) ;
#20717=CARTESIAN_POINT ( 'NONE',  ( -41.33442610868027600, -25.31287256288777243, 5.287398422161111000 ) ) ;
#20718=ADVANCED_FACE ( 'NONE', ( #58308 ), #25840, .T. ) ;
#20719=CARTESIAN_POINT ( 'NONE',  ( -95.62721569424989809, -24.73486907724918282, 1.287355809206966128 ) ) ;
#20720=CARTESIAN_POINT ( 'NONE',  ( -99.50802124428108186, -24.66019654487200086, 8.947790411086117501 ) ) ;
#20721=CARTESIAN_POINT ( 'NONE',  ( 19.78805588120126302, 8.271231038663975355, 11.49999999999999645 ) ) ;
#20723=DIRECTION ( 'NONE',  ( -3.773278334453079030E-23, 0.9999999999976377785, 2.173523156925979128E-06 ) ) ;
#20724=ORIENTED_EDGE ( 'NONE', *, *, #48525, .T. ) ;
#20725=CARTESIAN_POINT ( 'NONE',  ( 19.22371909900314435, 11.20011194808016342, -1.500000000000002220 ) ) ;
#20726=CARTESIAN_POINT ( 'NONE',  ( 11.71144010791963730, -17.07555522294065753, 11.49999999999998934 ) ) ;
#20727=EDGE_CURVE ( 'NONE', #76683, #82898, #10658, .T. ) ;
#20730=CARTESIAN_POINT ( 'NONE',  ( -28.52392022028078600, -24.49901761805231359, 1.056161677404373611 ) ) ;
#20733=AXIS2_PLACEMENT_3D ( 'NONE', #84284, #93903, #14768 ) ;
#20735=CARTESIAN_POINT ( 'NONE',  ( 15.04517842881462819, -14.58609674458608829, -1.500000000000002220 ) ) ;
#20736=CARTESIAN_POINT ( 'NONE',  ( 18.42579859434530931, 11.83097890990371148, 11.49999999999999645 ) ) ;
#20737=CARTESIAN_POINT ( 'NONE',  ( -37.65706361072022901, -23.73791477778911485, 11.05961554403171121 ) ) ;
#20738=CARTESIAN_POINT ( 'NONE',  ( -22.13300264024875119, -4.194623038110560032, -1.500000000000002220 ) ) ;
#20739=CARTESIAN_POINT ( 'NONE',  ( 19.44712688777480736, 7.780496645421295376, 11.49999999999998934 ) ) ;
#20741=DIRECTION ( 'NONE',  ( -3.773278334444165844E-23, 1.000000000000000000, 0.000000000000000000 ) ) ;
#20742=CARTESIAN_POINT ( 'NONE',  ( -99.62287095715005592, -29.50250243563736774, 8.947779886222138046 ) ) ;
#20744=AXIS2_PLACEMENT_3D ( 'NONE', #8320, #47391, #93044 ) ;
#20745=ORIENTED_EDGE ( 'NONE', *, *, #31659, .T. ) ;
#20746=ORIENTED_EDGE ( 'NONE', *, *, #58990, .T. ) ;
#20748=CARTESIAN_POINT ( 'NONE',  ( -21.39523464106120088, -1.845724655749456433, -1.500000000000002220 ) ) ;
#20749=CARTESIAN_POINT ( 'NONE',  ( -88.62287095715004170, -24.64898659630367916, 1.056161002820827921 ) ) ;
#20750=ORIENTED_EDGE ( 'NONE', *, *, #30190, .T. ) ;
#20751=CARTESIAN_POINT ( 'NONE',  ( -11.89019930860364482, -17.45089671868802128, 11.49999999999998934 ) ) ;
#20752=CARTESIAN_POINT ( 'NONE',  ( -92.62287095715005592, -24.64965695001469115, 8.947790433994180503 ) ) ;
#20754=CARTESIAN_POINT ( 'NONE',  ( -83.52214250679790553, -23.48786465467241058, 11.44779295918254469 ) ) ;
#20756=CARTESIAN_POINT ( 'NONE',  ( -100.0362565971423976, -25.11991538313833416, 2.885717652640028330 ) ) ;
#20757=CARTESIAN_POINT ( 'NONE',  ( -2.767897998228395551, 21.91458177938747909, -1.500000000000002220 ) ) ;
#20758=DIRECTION ( 'NONE',  ( 0.000000000000000000, 2.173523156925980399E-06, -0.9999999999976378895 ) ) ;
#20761=FACE_OUTER_BOUND ( 'NONE', #15873, .T. ) ;
#20762=CARTESIAN_POINT ( 'NONE',  ( -12.45040968399260883, -14.89389333286084671, 11.49999999999998934 ) ) ;
#20763=CARTESIAN_POINT ( 'NONE',  ( 2.936642053869352953, -21.15864249054145674, 11.49999999999998934 ) ) ;
#20765=CARTESIAN_POINT ( 'NONE',  ( -121.6228709571500417, -29.50248528299804818, 1.056150453629045360 ) ) ;
#20766=CARTESIAN_POINT ( 'NONE',  ( -64.55954184534172668, -23.73791477778911840, 11.05961554403170766 ) ) ;
#20767=CARTESIAN_POINT ( 'NONE',  ( -40.52287095715006870, -29.50247984919015209, -1.443849546365060466 ) ) ;
#20768=CARTESIAN_POINT ( 'NONE',  ( 9.629844747126790949, -20.51516216672183290, -1.500000000000002220 ) ) ;
#20769=B_SPLINE_SURFACE_WITH_KNOTS ( 'NONE', 3, 3, ( 
 ( #68391, #15094, #21691, #99323 ),
 ( #92215, #44553, #69385, #54180 ),
 ( #46060, #15587, #6489, #29818 ),
 ( #85104, #77480, #98824, #60291 ),
 ( #90725, #22688, #30823, #76479 ),
 ( #100304, #36932, #21198, #52165 ),
 ( #7981, #5983, #37933, #13585 ) ),
 .UNSPECIFIED., .F., .F., .F.,
 ( 4, 3, 4 ),
 ( 4, 4 ),
 ( 0.7945040050992241421, 0.8970133687736501216, 0.9995227324480761011 ),
 ( 0.4296031653624693414, 0.4308142232466789512 ),
 .UNSPECIFIED. ) ;
#20770=ORIENTED_EDGE ( 'NONE', *, *, #64265, .T. ) ;
#20771=CARTESIAN_POINT ( 'NONE',  ( -87.52287095715007581, -23.73934037231757088, 11.05740245334328620 ) ) ;
#20772=CARTESIAN_POINT ( 'NONE',  ( -104.5562042904834072, -24.64965694238574656, 8.947790433994192938 ) ) ;
#20773=CARTESIAN_POINT ( 'NONE',  ( 0.4224338394261131779, -19.80333402765648998, 11.49999999999999645 ) ) ;
#20776=DIRECTION ( 'NONE',  ( -3.773278334453079618E-23, 0.9999999999976377785, 2.173523156925979975E-06 ) ) ;
#20777=ORIENTED_EDGE ( 'NONE', *, *, #91804, .T. ) ;
#20778=CARTESIAN_POINT ( 'NONE',  ( -59.52287095715007581, -24.33832256527048088, 0.1851278514138623987 ) ) ;
#20779=CARTESIAN_POINT ( 'NONE',  ( -29.79725469281722994, -25.26026879864525654, 4.359877333242863529 ) ) ;
#20781=CARTESIAN_POINT ( 'NONE',  ( -100.6597906528727577, -25.17353340775167680, 7.087518319904864583 ) ) ;
#20782=CARTESIAN_POINT ( 'NONE',  ( -20.67203406374276398, -6.343553224398504220, -1.500000000000002220 ) ) ;
#20785=CARTESIAN_POINT ( 'NONE',  ( -16.24122463664219396, 10.56255597858309869, -1.500000000000002220 ) ) ;
#20787=LINE ( 'NONE', #97913, #35153 ) ;
#20789=CARTESIAN_POINT ( 'NONE',  ( -17.21045110277357182, -9.822940424218707278, -1.500000000000002220 ) ) ;
#20790=ORIENTED_EDGE ( 'NONE', *, *, #74726, .F. ) ;
#20791=EDGE_CURVE ( 'NONE', #99871, #90203, #42087, .T. ) ;
#20792=CARTESIAN_POINT ( 'NONE',  ( 20.17645099164838030, 1.678240329834772115, 11.49999999999999645 ) ) ;
#20795=DIRECTION ( 'NONE',  ( -1.000000000000000000, -3.773278334444166432E-23, -8.201307841325785021E-29 ) ) ;
#20796=VERTEX_POINT ( 'NONE', #74023 ) ;
#20802=B_SPLINE_CURVE_WITH_KNOTS ( 'NONE', 3,
 ( #46673, #22306, #84212, #7097 ),
 .UNSPECIFIED., .F., .F.,
 ( 4, 4 ),
 ( 0.7910648800674725534, 0.8000713113395880871 ),
 .UNSPECIFIED. ) ;
#20803=LINE ( 'NONE', #6588, #88365 ) ;
#20804=CARTESIAN_POINT ( 'NONE',  ( -7.287290609967129740, 18.71191762695291771, 11.49999999999998934 ) ) ;
#20809=CARTESIAN_POINT ( 'NONE',  ( 9.198035947750891950, -20.93187084735588144, 11.49999999999999645 ) ) ;
#20811=CARTESIAN_POINT ( 'NONE',  ( -65.52287095715006160, -29.50248789122583659, 2.256150453626215580 ) ) ;
#20812=CARTESIAN_POINT ( 'NONE',  ( -53.58953762381673158, -23.47593901973091235, -1.443836447539009749 ) ) ;
#20814=B_SPLINE_CURVE_WITH_KNOTS ( 'NONE', 3,
 ( #95668, #73336, #34768, #96660, #25649, #27157, #2329, #88060 ),
 .UNSPECIFIED., .F., .F.,
 ( 4, 2, 2, 4 ),
 ( 6.384118695052880424E-06, 0.002007151183515480143, 0.003007534715925692069, 0.004007918248335903995 ),
 .UNSPECIFIED. ) ;
#20815=CARTESIAN_POINT ( 'NONE',  ( -118.6228709571500559, -23.73934037231758154, 11.05740245334328442 ) ) ;
#20816=CARTESIAN_POINT ( 'NONE',  ( -21.57557905285345612, -6.117077608415351087, 11.49999999999999645 ) ) ;
#20818=ORIENTED_EDGE ( 'NONE', *, *, #26672, .F. ) ;
#20819=CARTESIAN_POINT ( 'NONE',  ( -13.67433444753018534, -15.09191755960682890, 11.49999999999998934 ) ) ;
#20821=EDGE_CURVE ( 'NONE', #33585, #25851, #83243, .T. ) ;
#20822=CARTESIAN_POINT ( 'NONE',  ( 19.00551534866085746, 12.86435971046890359, -1.500000000000002220 ) ) ;
#20824=ORIENTED_EDGE ( 'NONE', *, *, #84965, .F. ) ;
#20825=PLANE ( 'NONE',  #75213 ) ;
#20826=CARTESIAN_POINT ( 'NONE',  ( -77.58171905157765025, -24.66019654487200441, 8.947790411086108620 ) ) ;
#20828=DIRECTION ( 'NONE',  ( -3.773278334453079618E-23, 0.9999999999976377785, 2.173523156925978705E-06 ) ) ;
#20829=CARTESIAN_POINT ( 'NONE',  ( 20.79131504077403747, 4.132458064796619368, 11.49999999999999645 ) ) ;
#20832=CARTESIAN_POINT ( 'NONE',  ( -20.56242917251232782, -8.299981740788712870, 11.49999999999998934 ) ) ;
#20833=CARTESIAN_POINT ( 'NONE',  ( 20.22723401096548201, -3.897675682603606084, -1.500000000000002220 ) ) ;
#20834=VERTEX_POINT ( 'NONE', #49202 ) ;
#20835=VERTEX_POINT ( 'NONE', #95854 ) ;
#20837=EDGE_CURVE ( 'NONE', #49749, #53188, #67634, .T. ) ;
#20841=AXIS2_PLACEMENT_3D ( 'NONE', #42337, #88493, #86979 ) ;
#20842=VERTEX_POINT ( 'NONE', #57320 ) ;
#20846=CARTESIAN_POINT ( 'NONE',  ( 16.28047541435887879, -12.87082401369967677, -1.500000000000002220 ) ) ;
#20847=CARTESIAN_POINT ( 'NONE',  ( -4.559408409702599307, -21.23122434433648209, 11.49999999999999645 ) ) ;
#20850=CARTESIAN_POINT ( 'NONE',  ( -51.84906229995659288, -25.19414663990379921, 6.647105277450162220 ) ) ;
#20851=CARTESIAN_POINT ( 'NONE',  ( -52.52287095715008292, -23.94994826722564341, -0.6494450866342716955 ) ) ;
#20852=CARTESIAN_POINT ( 'NONE',  ( -115.5589192835139727, -23.48783264082477018, -1.443836473390087916 ) ) ;
#20853=CARTESIAN_POINT ( 'NONE',  ( -21.98280116189361877, -4.439423430357301470, -1.500000000000002220 ) ) ;
#20855=B_SPLINE_CURVE_WITH_KNOTS ( 'NONE', 3,
 ( #63580, #40224, #71177, #48343 ),
 .UNSPECIFIED., .F., .F.,
 ( 4, 4 ),
 ( 0.7703360025610563877, 0.7793424338331719214 ),
 .UNSPECIFIED. ) ;
#20856=CARTESIAN_POINT ( 'NONE',  ( -51.19090461678316473, -25.31296676361253617, 4.328065606197115223 ) ) ;
#20857=CARTESIAN_POINT ( 'NONE',  ( -65.53457423475654764, -24.83618233451449697, 1.606449574219540155 ) ) ;
#20859=CARTESIAN_POINT ( 'NONE',  ( -59.52287095715006160, -24.64965694238407323, 8.947790433994201820 ) ) ;
#20860=CARTESIAN_POINT ( 'NONE',  ( -50.78505292327133702, -25.11974106722812650, 2.884744560678632830 ) ) ;
#20864=DIRECTION ( 'NONE',  ( 1.000000000000000000, 3.773278334444166432E-23, 8.201307841325785021E-29 ) ) ;
#20866=VERTEX_POINT ( 'NONE', #5501 ) ;
#20867=CARTESIAN_POINT ( 'NONE',  ( 17.02398533174402218, 12.79255474601471043, -1.500000000000002220 ) ) ;
#20870=CARTESIAN_POINT ( 'NONE',  ( 21.45948982579844255, -4.128456637845983934, -1.500000000000002220 ) ) ;
#20871=CARTESIAN_POINT ( 'NONE',  ( -38.52287095715004739, -23.95044443724991368, 10.65354141964649237 ) ) ;
#20872=CARTESIAN_POINT ( 'NONE',  ( 22.16846167567618053, -4.910139430472912458, -1.500000000000002220 ) ) ;
#20874=CARTESIAN_POINT ( 'NONE',  ( -41.09701627025020088, -25.18430914849951918, 3.494173821712560635 ) ) ;
#20875=CARTESIAN_POINT ( 'NONE',  ( -123.6228709571500559, -24.64965695001469115, 8.947790433994175174 ) ) ;
#20876=CARTESIAN_POINT ( 'NONE',  ( -8.322136096487577461, -20.27582920440508829, -1.500000000000002220 ) ) ;
#20878=ORIENTED_EDGE ( 'NONE', *, *, #98727, .F. ) ;
#20879=CARTESIAN_POINT ( 'NONE',  ( -40.25461668630514112, -25.29393289446231918, 5.534671799676078585 ) ) ;
#20883=CARTESIAN_POINT ( 'NONE',  ( -0.1051616404667209126, -21.68859992388199487, -0.4716817114508950470 ) ) ;
#20884=CARTESIAN_POINT ( 'NONE',  ( 16.87399902462237478, -12.92443306546820736, -1.500000000000002220 ) ) ;
#20885=CARTESIAN_POINT ( 'NONE',  ( -112.5569623344011632, -23.73766607897671577, -1.055555164236427368 ) ) ;
#20886=CARTESIAN_POINT ( 'NONE',  ( -26.09735693242928534, -24.97064964884102167, 4.864565919031297980 ) ) ;
#20887=CARTESIAN_POINT ( 'NONE',  ( -85.60742529143259105, -23.48783264082476308, -1.443836473390099018 ) ) ;
#20888=CARTESIAN_POINT ( 'NONE',  ( -33.57064321401880846, -23.48783264082477729, -1.443836473390078146 ) ) ;
#20890=B_SPLINE_CURVE_WITH_KNOTS ( 'NONE', 3,
 ( #2421, #89646, #41478, #65834 ),
 .UNSPECIFIED., .F., .F.,
 ( 4, 4 ),
 ( 0.000000000000000000, 9.999999999998897304E-05 ),
 .UNSPECIFIED. ) ;
#20891=CARTESIAN_POINT ( 'NONE',  ( -79.62287095715005592, -24.64965695001468404, 8.947790433994182280 ) ) ;
#20892=VERTEX_POINT ( 'NONE', #84121 ) ;
#20893=B_SPLINE_CURVE_WITH_KNOTS ( 'NONE', 3,
 ( #52880, #7695, #37646, #69604 ),
 .UNSPECIFIED., .F., .F.,
 ( 4, 4 ),
 ( 0.1498929593708818175, 0.1588993906429972958 ),
 .UNSPECIFIED. ) ;
#20894=CARTESIAN_POINT ( 'NONE',  ( 14.87128047407919951, 12.67365258641725312, 11.49999999999999645 ) ) ;
#20895=CARTESIAN_POINT ( 'NONE',  ( -108.5228709571500758, -23.95044443724992789, 10.65354141964648882 ) ) ;
#20896=EDGE_CURVE ( 'NONE', #11988, #85219, #85777, .T. ) ;
#20898=ORIENTED_EDGE ( 'NONE', *, *, #87824, .T. ) ;
#20899=DIRECTION ( 'NONE',  ( -3.773278334444167608E-23, 1.000000000000000000, 0.000000000000000000 ) ) ;
#20900=CARTESIAN_POINT ( 'NONE',  ( -99.19463651313202490, -25.31270078316470773, 5.270598708289442769 ) ) ;
#20902=CARTESIAN_POINT ( 'NONE',  ( -50.26656247056430260, -25.12363382914034560, 7.097961812911407264 ) ) ;
#20903=CARTESIAN_POINT ( 'NONE',  ( -0.8432318219891272726, -19.69000482574202238, 11.49999999999998934 ) ) ;
#20904=EDGE_LOOP ( 'NONE', ( #41484, #36966, #49233, #63170 ) ) ;
#20906=CARTESIAN_POINT ( 'NONE',  ( -44.62287095715004881, -29.50250243563736774, 8.947779886222148704 ) ) ;
#20907=PLANE ( 'NONE',  #73924 ) ;
#20908=EDGE_CURVE ( 'NONE', #21078, #12640, #25009, .T. ) ;
#20910=ORIENTED_EDGE ( 'NONE', *, *, #36020, .F. ) ;
#20911=CARTESIAN_POINT ( 'NONE',  ( -72.52287095715007581, -24.65952944569304606, 1.056160979905697239 ) ) ;
#20912=CARTESIAN_POINT ( 'NONE',  ( -87.58953762381671027, -24.64965694238406613, 8.947790433994653014 ) ) ;
#20913=CARTESIAN_POINT ( 'NONE',  ( -50.52287095715006160, -29.50248528299804818, 1.056150453629033370 ) ) ;
#20914=CARTESIAN_POINT ( 'NONE',  ( -116.5228709571500616, -24.64898659630368627, 1.056161002820833028 ) ) ;
#20916=VECTOR ( 'NONE', #81496, 1000.000000000000114 ) ;
#20919=CARTESIAN_POINT ( 'NONE',  ( -107.6248367076318999, -24.51314013834315730, 0.6176544820404215042 ) ) ;
#20920=CARTESIAN_POINT ( 'NONE',  ( 13.89251353435424363, -14.32104260081073832, 11.49999999999998934 ) ) ;
#20922=CARTESIAN_POINT ( 'NONE',  ( -41.62287095715004881, -24.51387760970722240, 9.387446482453418284 ) ) ;
#20924=EDGE_LOOP ( 'NONE', ( #63865, #14351, #33987, #45452 ) ) ;
#20929=CARTESIAN_POINT ( 'NONE',  ( -106.6228709571500559, -23.47593901973091235, -1.443836447538999312 ) ) ;
#20931=CARTESIAN_POINT ( 'NONE',  ( -127.1719664006464257, -25.27146806274451407, 5.923224605469175508 ) ) ;
#20932=CARTESIAN_POINT ( 'NONE',  ( -39.61745222137281530, -23.48783264082476308, -1.443836473390098352 ) ) ;
#20934=CARTESIAN_POINT ( 'NONE',  ( -27.99826093239865443, -25.26026290525073392, 1.648429554944246478 ) ) ;
#20938=CARTESIAN_POINT ( 'NONE',  ( -127.5558937812824922, -23.96119346886880663, -0.6495511937832001426 ) ) ;
#20940=CARTESIAN_POINT ( 'NONE',  ( -19.34540493331696354, 6.066486871809979142, 11.49999999999998934 ) ) ;
#20941=CARTESIAN_POINT ( 'NONE',  ( -105.5895376238167103, -24.99156044556202971, 7.747789690856172307 ) ) ;
#20942=CARTESIAN_POINT ( 'NONE',  ( -49.62287095715006302, -24.34917612406837861, 0.1852690917426592920 ) ) ;
#20946=EDGE_CURVE ( 'NONE', #37715, #90955, #34731, .T. ) ;
#20948=CARTESIAN_POINT ( 'NONE',  ( -1.290058840521481454, 20.04182742388497473, -1.500000000000002220 ) ) ;
#20949=CARTESIAN_POINT ( 'NONE',  ( 20.48634023128459347, 4.603634630958829632, 11.49999999999999645 ) ) ;
#20950=LINE ( 'NONE', #52419, #56753 ) ;
#20951=CARTESIAN_POINT ( 'NONE',  ( -70.48846634784443665, -24.92592662359561118, 8.075495903017998245 ) ) ;
#20952=CARTESIAN_POINT ( 'NONE',  ( -13.58966412916292299, 17.40808962483262690, 11.49999999999998934 ) ) ;
#20953=CARTESIAN_POINT ( 'NONE',  ( -20.35906544237474236, -2.577633573104691322, -1.500000000000002220 ) ) ;
#20954=CARTESIAN_POINT ( 'NONE',  ( -75.52287095715006160, -29.50248789122583659, 2.256150453626215580 ) ) ;
#20956=CARTESIAN_POINT ( 'NONE',  ( -34.62287095715005592, -23.47593901973091235, -1.443836447539013301 ) ) ;
#20958=ORIENTED_EDGE ( 'NONE', *, *, #39107, .T. ) ;
#20960=B_SPLINE_SURFACE_WITH_KNOTS ( 'NONE', 3, 3, ( 
 ( #10559, #41520, #63879, #2967 ),
 ( #48648, #56261, #41024, #71977 ),
 ( #64384, #2459, #6443, #51627 ),
 ( #81579, #37399, #44005, #68347 ),
 ( #91666, #82068, #66369, #22145 ),
 ( #12050, #73963, #59744, #60744 ),
 ( #45019, #12554, #14038, #4461 ) ),
 .UNSPECIFIED., .F., .F., .F.,
 ( 4, 3, 4 ),
 ( 4, 4 ),
 ( 0.7945040050992234759, 0.8970133687736494554, 0.9995227324480753239 ),
 ( 0.2395548714580574556, 0.2406781904383525350 ),
 .UNSPECIFIED. ) ;
#20961=CARTESIAN_POINT ( 'NONE',  ( -31.54521099866208189, -24.15543982623907127, -0.2315651400026576545 ) ) ;
#20963=ORIENTED_EDGE ( 'NONE', *, *, #100352, .F. ) ;
#20964=CARTESIAN_POINT ( 'NONE',  ( -83.52287095715006160, -24.65952944569304606, 1.056160979905698794 ) ) ;
#20965=CARTESIAN_POINT ( 'NONE',  ( -80.62287095715007013, -23.47596703998600631, 11.44779298504227860 ) ) ;
#20967=CARTESIAN_POINT ( 'NONE',  ( -14.32454646668868747, 14.77526322620295929, -1.500000000000002220 ) ) ;
#20968=CARTESIAN_POINT ( 'NONE',  ( -13.10987527212420645, -17.12674121770768920, 11.49999999999999645 ) ) ;
#20969=EDGE_LOOP ( 'NONE', ( #51719, #4232, #13230, #46247 ) ) ;
#20970=CARTESIAN_POINT ( 'NONE',  ( -59.52287095715006160, -23.47596703998600631, 11.44779298504228926 ) ) ;
#20971=FACE_OUTER_BOUND ( 'NONE', #44259, .T. ) ;
#20972=CARTESIAN_POINT ( 'NONE',  ( 22.31825301297700648, 1.237144038376295274, -1.500000000000002220 ) ) ;
#20973=CARTESIAN_POINT ( 'NONE',  ( -80.05243144761681151, -25.12205794285693372, 7.021016987878912374 ) ) ;
#20977=CARTESIAN_POINT ( 'NONE',  ( -51.22110488517359528, -25.30467804217069272, 4.840842006535183373 ) ) ;
#20978=CARTESIAN_POINT ( 'NONE',  ( 2.299058169534009100, 20.76012671103276475, -1.500000000000002220 ) ) ;
#20981=ADVANCED_FACE ( 'NONE', ( #15110 ), #52681, .T. ) ;
#20982=CARTESIAN_POINT ( 'NONE',  ( -67.50091646733569917, -24.35071581493543746, 9.817618358456023486 ) ) ;
#20985=CARTESIAN_POINT ( 'NONE',  ( -100.5894357946910418, -24.52399227489127398, 9.353111116836521077 ) ) ;
#20986=CARTESIAN_POINT ( 'NONE',  ( 20.24497096899912307, 5.935080660949433096, -1.500000000000002220 ) ) ;
#20987=VERTEX_POINT ( 'NONE', #22207 ) ;
#20990=CARTESIAN_POINT ( 'NONE',  ( -61.58953762381671737, -23.48786465467240347, 11.44779295918254824 ) ) ;
#20993=CARTESIAN_POINT ( 'NONE',  ( -50.22113196962826720, -25.11144614215787385, 2.838499443990665227 ) ) ;
#20994=CARTESIAN_POINT ( 'NONE',  ( 6.244050601037331560, 20.82503750550150912, -1.500000000000002220 ) ) ;
#20995=CARTESIAN_POINT ( 'NONE',  ( -79.70858743522369139, -25.08277761643740789, 7.371951261098620201 ) ) ;
#20996=CARTESIAN_POINT ( 'NONE',  ( 7.190675130926929448, -21.12231643677837312, 11.49999999999999645 ) ) ;
#20998=CARTESIAN_POINT ( 'NONE',  ( -33.52287095715006160, -24.65952944569303895, 1.056160979905690134 ) ) ;
#21002=EDGE_CURVE ( 'NONE', #8368, #92960, #46076, .T. ) ;
#21004=EDGE_CURVE ( 'NONE', #34952, #46589, #63877, .T. ) ;
#21005=VERTEX_POINT ( 'NONE', #75498 ) ;
#21007=EDGE_CURVE ( 'NONE', #57610, #58811, #14606, .T. ) ;
#21008=AXIS2_PLACEMENT_3D ( 'NONE', #80708, #27425, #79698 ) ;
#21011=CARTESIAN_POINT ( 'NONE',  ( -49.62287095715005592, -29.50248528299804818, 1.056150453629033370 ) ) ;
#21012=CARTESIAN_POINT ( 'NONE',  ( -49.74369414166533687, -25.31543073408252909, 4.940877929217667663 ) ) ;
#21013=VECTOR ( 'NONE', #24492, 1000.000000000000114 ) ;
#21014=FACE_OUTER_BOUND ( 'NONE', #46222, .T. ) ;
#21016=VERTEX_POINT ( 'NONE', #60307 ) ;
#21017=CARTESIAN_POINT ( 'NONE',  ( 17.72857150710123619, 7.855407458714720903, 11.49999999999999645 ) ) ;
#21019=EDGE_CURVE ( 'NONE', #51364, #64821, #23717, .T. ) ;
#21020=ORIENTED_EDGE ( 'NONE', *, *, #22599, .T. ) ;
#21021=DIRECTION ( 'NONE',  ( 0.000000000000000000, 0.9999999999976377785, 2.173523156925979128E-06 ) ) ;
#21023=DIRECTION ( 'NONE',  ( 3.773278334444167608E-23, -1.000000000000000000, 0.000000000000000000 ) ) ;
#21024=LINE ( 'NONE', #53994, #24456 ) ;
#21025=CARTESIAN_POINT ( 'NONE',  ( -19.37001648656083574, -3.113731218521536004, -1.500000000000002220 ) ) ;
#21026=CARTESIAN_POINT ( 'NONE',  ( -46.63380027522481441, -24.34968618360932879, 0.1864209137778778391 ) ) ;
#21027=VERTEX_POINT ( 'NONE', #48588 ) ;
#21028=CARTESIAN_POINT ( 'NONE',  ( -21.01953065494444317, -4.859126342152997324, 11.49999999999998934 ) ) ;
#21029=CARTESIAN_POINT ( 'NONE',  ( -33.60141092905455196, -23.96169478059712432, 10.65365249895719124 ) ) ;
#21030=CARTESIAN_POINT ( 'NONE',  ( -61.64687923781919920, -25.20074463982482982, 3.409327697717700278 ) ) ;
#21031=CARTESIAN_POINT ( 'NONE',  ( -100.6228709571500559, -23.48783264082478794, -1.443836473390061936 ) ) ;
#21032=LINE ( 'NONE', #52003, #84450 ) ;
#21033=CARTESIAN_POINT ( 'NONE',  ( 17.37538969058663696, -15.08583811485692117, -1.500000000000002220 ) ) ;
#21037=DIRECTION ( 'NONE',  ( -3.773278334453079030E-23, 0.9999999999976377785, 2.173523156925979128E-06 ) ) ;
#21038=CARTESIAN_POINT ( 'NONE',  ( -50.10347978215904874, -25.18370859199909972, 3.285367768258824483 ) ) ;
#21039=CARTESIAN_POINT ( 'NONE',  ( 6.436487395234643749, 19.08016507665710648, 11.49999999999999645 ) ) ;
#21041=CARTESIAN_POINT ( 'NONE',  ( -32.56126148258746156, -23.73791477778911485, 11.05961554403171299 ) ) ;
#21042=CARTESIAN_POINT ( 'NONE',  ( -115.6228709571500559, -29.50250786944525672, 11.44777988621622811 ) ) ;
#21044=CARTESIAN_POINT ( 'NONE',  ( -122.5228709571500900, -24.35013146730204170, 9.818937971375095941 ) ) ;
#21045=CARTESIAN_POINT ( 'NONE',  ( -11.18921147948170614, -16.41150865552512883, -1.500000000000002220 ) ) ;
#21046=ADVANCED_FACE ( 'NONE', ( #94733 ), #58857, .T. ) ;
#21047=CARTESIAN_POINT ( 'NONE',  ( -113.5932511717749236, -23.73766607897670156, -1.055555164236448240 ) ) ;
#21048=CARTESIAN_POINT ( 'NONE',  ( -3.504374479207110316, 19.46862825742285708, -1.500000000000002220 ) ) ;
#21049=CARTESIAN_POINT ( 'NONE',  ( -126.6248985653323160, -23.73791477778912551, 11.05961554403169878 ) ) ;
#21050=EDGE_CURVE ( 'NONE', #14844, #65225, #86125, .T. ) ;
#21052=CARTESIAN_POINT ( 'NONE',  ( -37.52287095715007581, -24.34917612407031129, 0.1852690917476942090 ) ) ;
#21053=CARTESIAN_POINT ( 'NONE',  ( 15.58315679939408582, 13.61395703526229894, 11.49999999999999645 ) ) ;
#21056=LINE ( 'NONE', #68247, #73997 ) ;
#21057=CARTESIAN_POINT ( 'NONE',  ( -49.86018645952977835, -25.25138696836355834, 5.308912666256677682 ) ) ;
#21058=CARTESIAN_POINT ( 'NONE',  ( -22.42851769774927817, -3.676000928666301792, 11.49999999999999645 ) ) ;
#21060=CARTESIAN_POINT ( 'NONE',  ( -46.62287095715004170, -24.35013146730203815, 9.818937971375113705 ) ) ;
#21061=CARTESIAN_POINT ( 'NONE',  ( -62.62287095715004881, -23.47593901973091235, -1.443836447539007972 ) ) ;
#21062=AXIS2_PLACEMENT_3D ( 'NONE', #19844, #73651, #96483 ) ;
#21066=AXIS2_PLACEMENT_3D ( 'NONE', #88677, #74439, #4932 ) ;
#21068=ORIENTED_EDGE ( 'NONE', *, *, #21138, .T. ) ;
#21070=CARTESIAN_POINT ( 'NONE',  ( -98.58953762381673869, -23.47596703998600631, 11.44779298504227683 ) ) ;
#21071=CARTESIAN_POINT ( 'NONE',  ( 22.56601425305882813, -3.627385684441148506, -1.500000000000002220 ) ) ;
#21072=CARTESIAN_POINT ( 'NONE',  ( -29.48781380955602316, -24.26270740365838208, 0.1864212292069160337 ) ) ;
#21073=VECTOR ( 'NONE', #43002, 1000.000000000000114 ) ;
#21074=CARTESIAN_POINT ( 'NONE',  ( 10.28227983848843152, -18.94921665015282031, -1.500000000000002220 ) ) ;
#21076=CARTESIAN_POINT ( 'NONE',  ( -51.62287095715005592, -29.50250243563736774, 8.947779886222146928 ) ) ;
#21077=CARTESIAN_POINT ( 'NONE',  ( -14.53490578827140212, -17.26895500059623956, 11.49999999999999645 ) ) ;
#21078=VERTEX_POINT ( 'NONE', #93227 ) ;
#21080=CARTESIAN_POINT ( 'NONE',  ( -27.97282668350885615, -24.81073594632751522, 2.304836069181902314 ) ) ;
#21081=CARTESIAN_POINT ( 'NONE',  ( -17.28599015371049674, 13.57978550619682956, 11.49999999999998934 ) ) ;
#21083=CARTESIAN_POINT ( 'NONE',  ( -105.6235594712198775, -25.00182538069147142, 7.747789668545044250 ) ) ;
#21084=CARTESIAN_POINT ( 'NONE',  ( -28.94649234366282187, -24.79700135719347642, 6.769413541375830512 ) ) ;
#21085=EDGE_CURVE ( 'NONE', #57610, #63805, #21400, .T. ) ;
#21088=CARTESIAN_POINT ( 'NONE',  ( -90.52212987707727621, -23.48786465467241769, 11.44779295918255180 ) ) ;
#21089=ORIENTED_EDGE ( 'NONE', *, *, #97883, .T. ) ;
#21090=CARTESIAN_POINT ( 'NONE',  ( -36.52287095715009002, -24.66019654487199730, 8.947790411086124607 ) ) ;
#21091=ORIENTED_EDGE ( 'NONE', *, *, #1690, .T. ) ;
#21092=VERTEX_POINT ( 'NONE', #8999 ) ;
#21094=LINE ( 'NONE', #83492, #69742 ) ;
#21095=CARTESIAN_POINT ( 'NONE',  ( -36.64923509539228519, -23.96119346886880663, -0.6495511937832127991 ) ) ;
#21096=CARTESIAN_POINT ( 'NONE',  ( -19.37329759448073574, 6.469241145865432863, -1.500000000000002220 ) ) ;
#21099=CARTESIAN_POINT ( 'NONE',  ( -92.52287095715006160, -24.35013146730203815, 9.818937971375097717 ) ) ;
#21104=FACE_OUTER_BOUND ( 'NONE', #48236, .T. ) ;
#21105=CARTESIAN_POINT ( 'NONE',  ( 11.56195852851363526, -17.29799701895051811, -1.500000000000002220 ) ) ;
#21106=VERTEX_POINT ( 'NONE', #39952 ) ;
#21108=ORIENTED_EDGE ( 'NONE', *, *, #72008, .F. ) ;
#21109=EDGE_CURVE ( 'NONE', #27009, #43974, #14220, .T. ) ;
#21111=DIRECTION ( 'NONE',  ( 0.000000000000000000, 0.9999999999976377785, 2.173523156925979128E-06 ) ) ;
#21112=ORIENTED_EDGE ( 'NONE', *, *, #5680, .T. ) ;
#21114=DIRECTION ( 'NONE',  ( -3.773278334453079618E-23, 0.9999999999976377785, 2.173523156925979975E-06 ) ) ;
#21115=CARTESIAN_POINT ( 'NONE',  ( -119.4728709571500360, -25.30558663486607429, 5.000950657679038791 ) ) ;
#21117=CARTESIAN_POINT ( 'NONE',  ( -95.52287095715006160, -23.47596703998600631, 11.44779298504228215 ) ) ;
#21118=CARTESIAN_POINT ( 'NONE',  ( -14.73459587841175633, -16.56598928932902837, 11.49999999999999645 ) ) ;
#21119=ORIENTED_EDGE ( 'NONE', *, *, #78074, .T. ) ;
#21120=CARTESIAN_POINT ( 'NONE',  ( -62.52287095715006160, -29.50250243563736774, 8.947779886222145151 ) ) ;
#21121=CARTESIAN_POINT ( 'NONE',  ( 6.494847429386178206, -21.66115869805930672, -1.500000000000002220 ) ) ;
#21124=EDGE_CURVE ( 'NONE', #37824, #46066, #98874, .T. ) ;
#21125=CARTESIAN_POINT ( 'NONE',  ( -46.52287095715004028, -24.66019654487199375, 8.947790411086122830 ) ) ;
#21127=ORIENTED_EDGE ( 'NONE', *, *, #11289, .F. ) ;
#21129=B_SPLINE_CURVE_WITH_KNOTS ( 'NONE', 3,
 ( #99450, #28444, #83234, #13717, #68028, #72411 ),
 .UNSPECIFIED., .F., .F.,
 ( 4, 2, 4 ),
 ( 0.000000000000000000, 0.001380901958385395483, 0.002761803916770790967 ),
 .UNSPECIFIED. ) ;
#21130=FACE_OUTER_BOUND ( 'NONE', #95023, .T. ) ;
#21131=VECTOR ( 'NONE', #68283, 1000.000000000000114 ) ;
#21132=CARTESIAN_POINT ( 'NONE',  ( -19.30929855918770954, 5.666966705251045511, 11.49999999999998934 ) ) ;
#21134=EDGE_LOOP ( 'NONE', ( #36755, #4636, #42983, #21163 ) ) ;
#21136=CARTESIAN_POINT ( 'NONE',  ( -14.60993195340527251, 16.82711592829100411, -1.500000000000002220 ) ) ;
#21138=EDGE_CURVE ( 'NONE', #89278, #25123, #89627, .T. ) ;
#21139=ORIENTED_EDGE ( 'NONE', *, *, #9737, .F. ) ;
#21140=LINE ( 'NONE', #50612, #77278 ) ;
#21141=CARTESIAN_POINT ( 'NONE',  ( -81.57013478349688285, -25.12715095569221901, 7.081260212053098080 ) ) ;
#21142=DIRECTION ( 'NONE',  ( -3.773278334453080206E-23, 0.9999999999976377785, 2.173523156925979975E-06 ) ) ;
#21143=CARTESIAN_POINT ( 'NONE',  ( -84.52287095715006160, -24.65952944569304606, 1.056160979905698794 ) ) ;
#21144=CARTESIAN_POINT ( 'NONE',  ( -73.62287095715005592, -24.64965695001468404, 8.947790433994184056 ) ) ;
#21145=EDGE_CURVE ( 'NONE', #83889, #11321, #22666, .T. ) ;
#21146=CARTESIAN_POINT ( 'NONE',  ( 1.133552453683672745, -19.47370032599940615, -1.500000000000002220 ) ) ;
#21147=AXIS2_PLACEMENT_3D ( 'NONE', #92862, #23339, #15742 ) ;
#21148=CARTESIAN_POINT ( 'NONE',  ( -7.042111407433782055, -20.27750348750624099, -1.500000000000002220 ) ) ;
#21150=CARTESIAN_POINT ( 'NONE',  ( -123.5228709571500616, -29.50250786944525672, 11.44777988621622811 ) ) ;
#21152=CARTESIAN_POINT ( 'NONE',  ( 12.37853024107498534, -19.16169124346054176, -1.500000000000002220 ) ) ;
#21153=ADVANCED_FACE ( 'NONE', ( #11998 ), #72591, .T. ) ;
#21156=AXIS2_PLACEMENT_3D ( 'NONE', #72477, #12053, #11067 ) ;
#21157=LINE ( 'NONE', #97299, #40210 ) ;
#21159=CARTESIAN_POINT ( 'NONE',  ( 16.79232260237064978, 10.84791536263152523, 11.49999999999999645 ) ) ;
#21160=CARTESIAN_POINT ( 'NONE',  ( -111.6228709571500559, -23.47593901973091235, -1.443836447538999312 ) ) ;
#21161=CARTESIAN_POINT ( 'NONE',  ( -74.53890682171518733, -24.66019654487200441, 8.947790411086105067 ) ) ;
#21162=CARTESIAN_POINT ( 'NONE',  ( -29.52287095715006160, -29.50248298729119867, -6.412432996800796609E-05 ) ) ;
#21163=ORIENTED_EDGE ( 'NONE', *, *, #80716, .F. ) ;
#21164=CARTESIAN_POINT ( 'NONE',  ( -57.52287095715008292, -23.47593901973090524, -1.443836447538997092 ) ) ;
#21166=EDGE_CURVE ( 'NONE', #31278, #45090, #43183, .T. ) ;
#21167=CARTESIAN_POINT ( 'NONE',  ( 21.56942612084361599, 2.798134137018522427, -1.500000000000002220 ) ) ;
#21169=CARTESIAN_POINT ( 'NONE',  ( 10.47639735327893362, 16.54961352017854637, -1.500000000000002220 ) ) ;
#21173=B_SPLINE_CURVE_WITH_KNOTS ( 'NONE', 3,
 ( #41001, #72453, #19147, #73944, #71958, #2439, #4441, #50607 ),
 .UNSPECIFIED., .F., .F.,
 ( 4, 2, 2, 4 ),
 ( -0.001224554619866347364, -0.0002241820295893646661, 0.0007761905606876180318, 0.002776935741241578874 ),
 .UNSPECIFIED. ) ;
#21178=CARTESIAN_POINT ( 'NONE',  ( 15.48611046165106941, -13.43736321338083783, 11.49999999999999645 ) ) ;
#21180=CARTESIAN_POINT ( 'NONE',  ( -54.22287095715006444, -23.47596703998600276, 11.44779298504227683 ) ) ;
#21181=ORIENTED_EDGE ( 'NONE', *, *, #80161, .F. ) ;
#21183=CARTESIAN_POINT ( 'NONE',  ( -39.67258447180102365, -25.28892493200908476, 3.621101239112743730 ) ) ;
#21186=VERTEX_POINT ( 'NONE', #12987 ) ;
#21188=CARTESIAN_POINT ( 'NONE',  ( -1.973530150111237003, 22.95712487800313539, 11.49999999999999645 ) ) ;
#21189=CARTESIAN_POINT ( 'NONE',  ( -2.506051680461856890, -22.62920675306992280, 11.49999999999998934 ) ) ;
#21190=LINE ( 'NONE', #75470, #38904 ) ;
#21191=CARTESIAN_POINT ( 'NONE',  ( -116.6228709571500417, -23.48786465467241769, 11.44779295918253759 ) ) ;
#21192=CARTESIAN_POINT ( 'NONE',  ( -49.76601615100549481, -25.22051099802980900, 3.484103503325944207 ) ) ;
#21193=CARTESIAN_POINT ( 'NONE',  ( -115.5228709571500616, -23.48783264082477018, -1.443836473390083475 ) ) ;
#21194=CARTESIAN_POINT ( 'NONE',  ( -99.16166289166535819, -25.30157770236289139, 5.311370747789966984 ) ) ;
#21195=VECTOR ( 'NONE', #88024, 1000.000000000000114 ) ;
#21196=CARTESIAN_POINT ( 'NONE',  ( 20.57945552106664877, -7.502658216658728563, 11.49999999999998934 ) ) ;
#21198=CARTESIAN_POINT ( 'NONE',  ( -87.55830585607125727, -23.73791477778911840, 11.05961554403170588 ) ) ;
#21199=CARTESIAN_POINT ( 'NONE',  ( -77.62287095715005592, -24.34917612406838217, 0.1852690917426639272 ) ) ;
#21201=DIRECTION ( 'NONE',  ( -1.000000000000000000, -3.773278334444166432E-23, -8.201307841325785021E-29 ) ) ;
#21202=CARTESIAN_POINT ( 'NONE',  ( -86.62287095715005592, -23.72773821059536559, 11.05748984161097681 ) ) ;
#21203=ORIENTED_EDGE ( 'NONE', *, *, #37967, .T. ) ;
#21204=CARTESIAN_POINT ( 'NONE',  ( 1.945971545120378288, -20.36639758168144709, 11.49999999999998934 ) ) ;
#21205=ORIENTED_EDGE ( 'NONE', *, *, #36840, .F. ) ;
#21206=ORIENTED_EDGE ( 'NONE', *, *, #95520, .T. ) ;
#21209=B_SPLINE_CURVE_WITH_KNOTS ( 'NONE', 3,
 ( #53156, #14572, #97810, #59262 ),
 .UNSPECIFIED., .F., .F.,
 ( 4, 4 ),
 ( 0.000000000000000000, 1.000000000000000000 ),
 .UNSPECIFIED. ) ;
#21210=CARTESIAN_POINT ( 'NONE',  ( -19.45891602060003578, 12.32625358835968576, -1.500000000000002220 ) ) ;
#21211=FACE_OUTER_BOUND ( 'NONE', #3511, .T. ) ;
#21212=CARTESIAN_POINT ( 'NONE',  ( -6.636546740042271963, -19.09123619949631134, -1.500000000000002220 ) ) ;
#21213=ORIENTED_EDGE ( 'NONE', *, *, #6016, .T. ) ;
#21215=DIRECTION ( 'NONE',  ( 0.000000000000000000, 2.173523156925980399E-06, -0.9999999999976378895 ) ) ;
#21216=VECTOR ( 'NONE', #84915, 1000.000000000000114 ) ;
#21217=CARTESIAN_POINT ( 'NONE',  ( -31.62287095715005236, -24.64965695001467694, 8.947790433994189385 ) ) ;
#21218=CARTESIAN_POINT ( 'NONE',  ( -70.62545212654819693, -24.92564183028979130, 1.928384488918253536 ) ) ;
#21219=CARTESIAN_POINT ( 'NONE',  ( 13.27131465344908001, -16.79725507166503462, 11.49999999999999645 ) ) ;
#21220=ORIENTED_EDGE ( 'NONE', *, *, #24231, .F. ) ;
#21223=CARTESIAN_POINT ( 'NONE',  ( -19.01758589260300525, -8.224767016273846210, 11.49999999999998934 ) ) ;
#21224=EDGE_LOOP ( 'NONE', ( #47583, #69045, #21699, #16515 ) ) ;
#21225=DIRECTION ( 'NONE',  ( -3.773278334453079618E-23, 0.9999999999976377785, 2.173523156925979975E-06 ) ) ;
#21227=EDGE_CURVE ( 'NONE', #991, #57091, #45692, .T. ) ;
#21229=ORIENTED_EDGE ( 'NONE', *, *, #95946, .T. ) ;
#21230=EDGE_CURVE ( 'NONE', #23609, #59016, #6877, .T. ) ;
#21231=CARTESIAN_POINT ( 'NONE',  ( -20.92093621315066443, -1.481899440790641842, -1.500000000000002220 ) ) ;
#21232=CARTESIAN_POINT ( 'NONE',  ( 10.99670386783381737, -19.00842362925918749, 11.49999999999999645 ) ) ;
#21233=EDGE_CURVE ( 'NONE', #99101, #48827, #23868, .T. ) ;
#21234=CARTESIAN_POINT ( 'NONE',  ( -37.53880256316359976, -24.35071581493542325, 9.817618358456030592 ) ) ;
#21235=CARTESIAN_POINT ( 'NONE',  ( 14.28312119630281174, -17.39864199977734671, 11.49999999999998934 ) ) ;
#21237=CARTESIAN_POINT ( 'NONE',  ( -20.70934228997045068, 3.328930095467914185, 11.49999999999998934 ) ) ;
#21239=EDGE_CURVE ( 'NONE', #82905, #34088, #78385, .T. ) ;
#21240=CARTESIAN_POINT ( 'NONE',  ( -29.62287095715004881, -23.40875089534885589, 11.44779299594469713 ) ) ;
#21241=CARTESIAN_POINT ( 'NONE',  ( -53.58953762381671737, -23.48786465467241058, 11.44779295918255002 ) ) ;
#21244=ORIENTED_EDGE ( 'NONE', *, *, #44403, .F. ) ;
#21245=CARTESIAN_POINT ( 'NONE',  ( -42.62287095715004881, -24.65952944569303895, 1.056160979905691688 ) ) ;
#21246=CARTESIAN_POINT ( 'NONE',  ( -8.581294335678165908, -19.67629172487136557, -1.500000000000002220 ) ) ;
#21249=CARTESIAN_POINT ( 'NONE',  ( -11.89019930860364482, -17.45089671868802128, -1.500000000000002220 ) ) ;
#21251=CARTESIAN_POINT ( 'NONE',  ( -64.54381262529305729, -24.34968618360933235, 0.1864209137778785330 ) ) ;
#21252=CARTESIAN_POINT ( 'NONE',  ( -83.50989887316418958, -24.15620529776628089, 10.23563542870660470 ) ) ;
#21254=LINE ( 'NONE', #13642, #61658 ) ;
#21255=CARTESIAN_POINT ( 'NONE',  ( -4.051365815588555463, -21.74199345402511696, -1.500000000000002220 ) ) ;
#21256=CARTESIAN_POINT ( 'NONE',  ( -110.9909297185884327, -25.14264188228929697, 6.986250900936915365 ) ) ;
#21258=CARTESIAN_POINT ( 'NONE',  ( -56.52287095715006160, -23.95044443724991723, 10.65354141964649592 ) ) ;
#21259=CARTESIAN_POINT ( 'NONE',  ( -67.62287095715005592, -29.50250786944525672, 11.44777988621623699 ) ) ;
#21260=CARTESIAN_POINT ( 'NONE',  ( -83.52287095715006160, -23.47593901973090524, -1.443836447538996648 ) ) ;
#21261=CARTESIAN_POINT ( 'NONE',  ( -100.5143560509806377, -24.15503026093913874, -0.2815557561904538653 ) ) ;
#21262=EDGE_CURVE ( 'NONE', #68431, #48449, #32402, .T. ) ;
#21263=CARTESIAN_POINT ( 'NONE',  ( -11.04204518803028456, 15.98388583709530941, -1.500000000000002220 ) ) ;
#21264=CARTESIAN_POINT ( 'NONE',  ( 15.12546962493697933, 15.13007008128210096, 11.49999999999998934 ) ) ;
#21265=CARTESIAN_POINT ( 'NONE',  ( -69.89335126754821204, -25.05732033941839987, 7.496320311188993557 ) ) ;
#21266=LINE ( 'NONE', #30388, #51175 ) ;
#21270=CARTESIAN_POINT ( 'NONE',  ( -8.787219534579676861, -20.84281209399103929, -1.500000000000002220 ) ) ;
#21271=ORIENTED_EDGE ( 'NONE', *, *, #39975, .T. ) ;
#21274=CARTESIAN_POINT ( 'NONE',  ( -17.59554656748941071, 9.132484154288260214, 11.49999999999999645 ) ) ;
#21275=CARTESIAN_POINT ( 'NONE',  ( -108.6228709571500559, -24.64898659630368627, 1.056161002820831474 ) ) ;
#21276=B_SPLINE_CURVE_WITH_KNOTS ( 'NONE', 3,
 ( #83162, #67962, #90789, #21258, #5050, #44616 ),
 .UNSPECIFIED., .F., .F.,
 ( 4, 2, 4 ),
 ( 0.000000000000000000, 0.001380901958385387027, 0.002761803916770774053 ),
 .UNSPECIFIED. ) ;
#21277=B_SPLINE_CURVE_WITH_KNOTS ( 'NONE', 3,
 ( #78714, #79233, #9731, #40687, #33072, #94964 ),
 .UNSPECIFIED., .F., .F.,
 ( 4, 2, 4 ),
 ( 6.391158118970788496E-06, 0.001387004593080789615, 0.002767618028042608501 ),
 .UNSPECIFIED. ) ;
#21278=CARTESIAN_POINT ( 'NONE',  ( -119.5228709571500758, -24.51283580621365488, 0.6167428607019762588 ) ) ;
#21279=ORIENTED_EDGE ( 'NONE', *, *, #62501, .F. ) ;
#21281=CARTESIAN_POINT ( 'NONE',  ( -79.62287095715005592, -23.48783264082478794, -1.443836473390065489 ) ) ;
#21282=CARTESIAN_POINT ( 'NONE',  ( -92.52287095715006160, -24.64898659630529210, 1.056161002820827921 ) ) ;
#21283=CARTESIAN_POINT ( 'NONE',  ( 2.319523670979641849, -21.48760272935114557, 11.49999999999998934 ) ) ;
#21284=CARTESIAN_POINT ( 'NONE',  ( -27.68651082257923335, -24.79949475646172630, 7.605672536963987262 ) ) ;
#21285=CARTESIAN_POINT ( 'NONE',  ( -66.52287095715003318, -23.73934037231755667, 11.05740245334329153 ) ) ;
#21287=CARTESIAN_POINT ( 'NONE',  ( -51.62287095715005592, -29.50250786944525672, 11.44777988621624054 ) ) ;
#21289=CARTESIAN_POINT ( 'NONE',  ( -19.78623529325263775, -1.157695164950638844, -1.500000000000002220 ) ) ;
#21290=AXIS2_PLACEMENT_3D ( 'NONE', #19286, #57882, #35533 ) ;
#21293=CARTESIAN_POINT ( 'NONE',  ( 10.94010344783756672, -17.16519937159427656, 11.49999999999999645 ) ) ;
#21295=ADVANCED_FACE ( 'NONE', ( #70780 ), #48253, .T. ) ;
#21298=FACE_OUTER_BOUND ( 'NONE', #61722, .T. ) ;
#21299=CARTESIAN_POINT ( 'NONE',  ( -102.5895376238166961, -23.48783264082478794, -1.443836473390062158 ) ) ;
#21300=DIRECTION ( 'NONE',  ( 0.000000000000000000, -2.173523156925980399E-06, 0.9999999999976378895 ) ) ;
#21301=DIRECTION ( 'NONE',  ( -3.773278334453079030E-23, 0.9999999999976377785, 2.173523156925979128E-06 ) ) ;
#21303=CARTESIAN_POINT ( 'NONE',  ( 4.397486433803790007, -19.56896378179033036, -1.500000000000002220 ) ) ;
#21304=DIRECTION ( 'NONE',  ( -3.773278334453079618E-23, 0.9999999999976377785, 2.173523156925979975E-06 ) ) ;
#21306=CARTESIAN_POINT ( 'NONE',  ( -73.62287095715007013, -23.47596703998600276, 11.44779298504227860 ) ) ;
#21307=CARTESIAN_POINT ( 'NONE',  ( 2.581029390964978187, -22.66945732913600509, 11.49999999999999645 ) ) ;
#21308=CARTESIAN_POINT ( 'NONE',  ( -30.47287095715008576, -25.09213182968271028, 2.762438726437805858 ) ) ;
#21309=PLANE ( 'NONE',  #41315 ) ;
#21310=CARTESIAN_POINT ( 'NONE',  ( -90.52287095715006160, -23.47596703998600631, 11.44779298504228393 ) ) ;
#21311=B_SPLINE_CURVE_WITH_KNOTS ( 'NONE', 3,
 ( #76540, #99874, #75049, #69946, #32387, #31387 ),
 .UNSPECIFIED., .F., .F.,
 ( 4, 2, 4 ),
 ( 1.570755371633915156E-05, 0.001396183895866088620, 0.002776660238015838181 ),
 .UNSPECIFIED. ) ;
#21313=CARTESIAN_POINT ( 'NONE',  ( -43.52287095715006160, -24.64965694238406613, 8.947790433994205372 ) ) ;
#21315=CARTESIAN_POINT ( 'NONE',  ( -50.78043790469551055, -25.30419751004783890, 5.186272124421679841 ) ) ;
#21316=ORIENTED_EDGE ( 'NONE', *, *, #4536, .F. ) ;
#21317=CARTESIAN_POINT ( 'NONE',  ( -2.495337616714382367, -20.20711602426958819, -1.500000000000002220 ) ) ;
#21318=ORIENTED_EDGE ( 'NONE', *, *, #52014, .T. ) ;
#21319=CARTESIAN_POINT ( 'NONE',  ( 17.43399715339889511, -14.94103553264482720, 11.49999999999998934 ) ) ;
#21320=CARTESIAN_POINT ( 'NONE',  ( -53.52287095715009002, -24.51387760970724727, 9.387446482453409402 ) ) ;
#21323=CARTESIAN_POINT ( 'NONE',  ( -94.52287095715011844, -23.48783264082477373, -1.443836473390087027 ) ) ;
#21325=CARTESIAN_POINT ( 'NONE',  ( -0.06837171988653999166, -21.26218376953697486, 11.49999999999999645 ) ) ;
#21326=ORIENTED_EDGE ( 'NONE', *, *, #62064, .T. ) ;
#21327=VERTEX_POINT ( 'NONE', #62179 ) ;
#21328=CARTESIAN_POINT ( 'NONE',  ( 7.527104757430762128, -20.84474501729809859, -1.500000000000002220 ) ) ;
#21330=CARTESIAN_POINT ( 'NONE',  ( -3.146292006899429783, -20.37002610441940220, -1.500000000000002220 ) ) ;
#21331=ORIENTED_EDGE ( 'NONE', *, *, #29669, .F. ) ;
#21332=EDGE_LOOP ( 'NONE', ( #84162, #58787, #60405, #86269 ) ) ;
#21334=CARTESIAN_POINT ( 'NONE',  ( -56.62287095715005592, -24.65952944569304250, 1.056160979905693464 ) ) ;
#21336=EDGE_CURVE ( 'NONE', #11878, #10895, #68703, .T. ) ;
#21338=DIRECTION ( 'NONE',  ( -3.773278334453079030E-23, 0.9999999999976377785, 2.173523156925979128E-06 ) ) ;
#21339=CARTESIAN_POINT ( 'NONE',  ( -41.48644761199398090, -24.51419770103157347, 9.386484678747180510 ) ) ;
#21340=CARTESIAN_POINT ( 'NONE',  ( -94.58953762381671027, -24.64965694238575011, 8.947790433994196491 ) ) ;
#21341=CARTESIAN_POINT ( 'NONE',  ( -11.59579830748209517, 17.24510332420730663, -1.500000000000002220 ) ) ;
#21342=CARTESIAN_POINT ( 'NONE',  ( 5.219777686717518961, -21.12652377152128480, 11.49999999999999645 ) ) ;
#21344=DIRECTION ( 'NONE',  ( 0.000000000000000000, -2.173523156925980399E-06, 0.9999999999976378895 ) ) ;
#21346=CARTESIAN_POINT ( 'NONE',  ( -115.6270136601075649, -24.40034930558991277, 0.3402023900116066257 ) ) ;
#21347=CARTESIAN_POINT ( 'NONE',  ( -8.519796113377745783, 20.75715399588506926, -1.500000000000002220 ) ) ;
#21349=CARTESIAN_POINT ( 'NONE',  ( -31.24388727629348494, -24.86441894802673147, 8.247789967202360017 ) ) ;
#21351=CARTESIAN_POINT ( 'NONE',  ( -59.52287095715006870, -24.33927499327855060, 9.819080762295822495 ) ) ;
#21353=CARTESIAN_POINT ( 'NONE',  ( -51.69717015115858061, -25.25631740715194340, 3.906071115062512700 ) ) ;
#21356=VERTEX_POINT ( 'NONE', #46946 ) ;
#21359=CARTESIAN_POINT ( 'NONE',  ( -46.50653488599488128, -23.96169478059712432, 10.65365249895718414 ) ) ;
#21360=ORIENTED_EDGE ( 'NONE', *, *, #71946, .F. ) ;
#21361=CARTESIAN_POINT ( 'NONE',  ( -11.06822068739258391, -18.21809710261049275, -1.500000000000002220 ) ) ;
#21363=CARTESIAN_POINT ( 'NONE',  ( -117.5228709571500758, -23.47596703998600631, 11.44779298504227860 ) ) ;
#21364=CARTESIAN_POINT ( 'NONE',  ( 4.297136154115697160, 20.59472113332480703, -1.500000000000002220 ) ) ;
#21366=CARTESIAN_POINT ( 'NONE',  ( -11.11902432501355342, 19.77583997595719367, -1.500000000000002220 ) ) ;
#21367=CARTESIAN_POINT ( 'NONE',  ( -110.4731799116023154, -25.19577767130133950, 3.299187155915005665 ) ) ;
#21369=CARTESIAN_POINT ( 'NONE',  ( 17.35060923807083810, -13.37414737355047656, -1.500000000000002220 ) ) ;
#21370=DIRECTION ( 'NONE',  ( 0.000000000000000000, 2.173523156925980399E-06, -0.9999999999976378895 ) ) ;
#21371=ORIENTED_EDGE ( 'NONE', *, *, #44763, .T. ) ;
#21373=CARTESIAN_POINT ( 'NONE',  ( -120.5228709571500474, -24.62226745350441703, 0.9660975649729574011 ) ) ;
#21375=CARTESIAN_POINT ( 'NONE',  ( -30.59901082992093535, -24.82988274811088658, 8.370978854367630007 ) ) ;
#21376=CARTESIAN_POINT ( 'NONE',  ( 21.17668642892995834, 2.279540523802085605, 11.49999999999998934 ) ) ;
#21377=CARTESIAN_POINT ( 'NONE',  ( -55.62287095715007723, -24.15516710230292929, 10.28746687063725851 ) ) ;
#21378=CARTESIAN_POINT ( 'NONE',  ( -54.52287095715005449, -23.47593901973090169, -1.443836447538997092 ) ) ;
#21379=CARTESIAN_POINT ( 'NONE',  ( -85.49848347818377192, -24.83618233451451118, 1.606449574219533272 ) ) ;
#21380=CARTESIAN_POINT ( 'NONE',  ( -33.50411885267913448, -23.96119346886880308, -0.6495511937832006977 ) ) ;
#21384=CARTESIAN_POINT ( 'NONE',  ( -99.51322475060698025, -25.09877457005609358, 7.289752353020987563 ) ) ;
#21385=CARTESIAN_POINT ( 'NONE',  ( -15.96901387740391343, -11.39031854172415947, 11.49999999999999645 ) ) ;
#21386=CARTESIAN_POINT ( 'NONE',  ( -75.55620429048337883, -24.99156044556202261, 7.747789690856173195 ) ) ;
#21387=DIRECTION ( 'NONE',  ( 1.000000000000000000, 3.773278334444167608E-23, 8.201307833595939069E-29 ) ) ;
#21388=ORIENTED_EDGE ( 'NONE', *, *, #86529, .F. ) ;
#21389=CARTESIAN_POINT ( 'NONE',  ( -70.27422298781921484, -25.30465073045868252, 4.851635164186505200 ) ) ;
#21390=CARTESIAN_POINT ( 'NONE',  ( -99.29687923781919778, -25.25095983749288919, 6.149712203964893042 ) ) ;
#21393=CARTESIAN_POINT ( 'NONE',  ( -5.312243195520525596, -18.98051080891723430, -1.500000000000002220 ) ) ;
#21400=B_SPLINE_CURVE_WITH_KNOTS ( 'NONE', 3,
 ( #31845, #16601, #47579, #78498 ),
 .UNSPECIFIED., .F., .F.,
 ( 4, 4 ),
 ( 0.000000000000000000, 9.999999999998897304E-05 ),
 .UNSPECIFIED. ) ;
#21406=CARTESIAN_POINT ( 'NONE',  ( -55.62373610541767732, -25.00158670708910336, 2.256160236439221034 ) ) ;
#21407=CARTESIAN_POINT ( 'NONE',  ( -118.5200172836564434, -23.96119346886881019, -0.6495511937832023630 ) ) ;
#21409=PLANE ( 'NONE',  #345 ) ;
#21410=LINE ( 'NONE', #28536, #81845 ) ;
#21411=CARTESIAN_POINT ( 'NONE',  ( -11.50144725928494438, 16.33591932373696665, 11.49999999999998934 ) ) ;
#21413=CARTESIAN_POINT ( 'NONE',  ( -45.57314203077795156, -25.00182538069146787, 7.747789668545045139 ) ) ;
#21414=ORIENTED_EDGE ( 'NONE', *, *, #55153, .F. ) ;
#21419=CARTESIAN_POINT ( 'NONE',  ( -66.52287095715006160, -24.65952944569304606, 1.056160979905697239 ) ) ;
#21420=CARTESIAN_POINT ( 'NONE',  ( -98.62287095715005592, -29.50250243563736774, 8.947779886222138046 ) ) ;
#21422=CARTESIAN_POINT ( 'NONE',  ( -81.62360513611031365, -24.65952944569304961, 1.056160979905703901 ) ) ;
#21427=CARTESIAN_POINT ( 'NONE',  ( -127.6234793005920380, -24.65952944569305316, 1.056160979905708341 ) ) ;
#21428=ORIENTED_EDGE ( 'NONE', *, *, #90335, .T. ) ;
#21429=CARTESIAN_POINT ( 'NONE',  ( -0.6865706486018943178, -20.24796467851281179, 11.49999999999998934 ) ) ;
#21430=VECTOR ( 'NONE', #33870, 1000.000000000000114 ) ;
#21431=CARTESIAN_POINT ( 'NONE',  ( -108.6228709571500559, -29.50250786944525672, 11.44777988621622988 ) ) ;
#21436=PLANE ( 'NONE',  #8127 ) ;
#21437=CARTESIAN_POINT ( 'NONE',  ( 7.329891291799937925, -18.66831812819665970, -1.500000000000002220 ) ) ;
#21438=CARTESIAN_POINT ( 'NONE',  ( 1.943494986365726485, -21.02143711168614004, 11.49999999999999645 ) ) ;
#21440=CARTESIAN_POINT ( 'NONE',  ( -70.60486560330774353, -23.85049219812685806, 10.88485053497527311 ) ) ;
#21441=CARTESIAN_POINT ( 'NONE',  ( -20.36895902721504825, -8.506870616244709637, 11.49999999999998934 ) ) ;
#21442=CARTESIAN_POINT ( 'NONE',  ( -0.1859688948871585645, 20.53422428922035081, 11.49999999999998934 ) ) ;
#21443=DIRECTION ( 'NONE',  ( -3.773278334453080206E-23, 0.9999999999976377785, 2.173523156925979975E-06 ) ) ;
#21446=CARTESIAN_POINT ( 'NONE',  ( -47.62287095715004881, -29.50250243563736774, 8.947779886222146928 ) ) ;
#21449=CARTESIAN_POINT ( 'NONE',  ( -117.5228709571500758, -24.64898659630368272, 1.056161002820833028 ) ) ;
#21451=B_SPLINE_CURVE_WITH_KNOTS ( 'NONE', 3,
 ( #88756, #98340, #27349, #59300, #52186, #59810 ),
 .UNSPECIFIED., .F., .F.,
 ( 4, 2, 4 ),
 ( 6.391158118967745954E-06, 0.001387004593080786363, 0.002767618028042605031 ),
 .UNSPECIFIED. ) ;
#21452=B_SPLINE_CURVE_WITH_KNOTS ( 'NONE', 3,
 ( #30559, #39170, #23944, #77718 ),
 .UNSPECIFIED., .F., .F.,
 ( 4, 4 ),
 ( 1.492656813173654180E-05, 0.002483556359836170454 ),
 .UNSPECIFIED. ) ;
#21453=ORIENTED_EDGE ( 'NONE', *, *, #2020, .T. ) ;
#21456=CARTESIAN_POINT ( 'NONE',  ( -76.58806799865949699, -24.34968618360934300, 0.1864209137778859160 ) ) ;
#21457=CARTESIAN_POINT ( 'NONE',  ( 14.24201292913401140, 14.87178044790754328, -1.500000000000002220 ) ) ;
#21458=CARTESIAN_POINT ( 'NONE',  ( 20.54099941694853726, 6.510794959084822864, 11.49999999999999645 ) ) ;
#21462=CARTESIAN_POINT ( 'NONE',  ( 22.34790896907852442, -0.4833156648990815651, -1.500000000000002220 ) ) ;
#21463=CARTESIAN_POINT ( 'NONE',  ( -93.52287095715010423, -24.33832256527049509, 0.1851278514138617326 ) ) ;
#21464=CARTESIAN_POINT ( 'NONE',  ( -84.50669220013847394, -24.34968618360934300, 0.1864209137778835013 ) ) ;
#21467=CARTESIAN_POINT ( 'NONE',  ( -35.62991077901555315, -24.83644354573578994, 8.397322867130093016 ) ) ;
#21468=AXIS2_PLACEMENT_3D ( 'NONE', #93539, #94547, #55007 ) ;
#21470=CARTESIAN_POINT ( 'NONE',  ( -18.00717387566553995, 10.56535500573724740, 11.49999999999998934 ) ) ;
#21472=EDGE_LOOP ( 'NONE', ( #26654, #15014, #58702, #86993 ) ) ;
#21473=CARTESIAN_POINT ( 'NONE',  ( -86.55452917198827834, -23.96119346886881374, -0.6495511937831903726 ) ) ;
#21474=VERTEX_POINT ( 'NONE', #26102 ) ;
#21476=CARTESIAN_POINT ( 'NONE',  ( -100.5858019367288136, -24.83644354573579349, 8.397322867130096569 ) ) ;
#21477=CARTESIAN_POINT ( 'NONE',  ( 18.35617536642501690, 10.39506492455470088, -1.500000000000002220 ) ) ;
#21478=ORIENTED_EDGE ( 'NONE', *, *, #17837, .T. ) ;
#21481=CARTESIAN_POINT ( 'NONE',  ( -21.74948284930419717, -1.071797830193938372, 11.49999999999998934 ) ) ;
#21482=CARTESIAN_POINT ( 'NONE',  ( -72.62287095715005592, -23.47593901973091235, -1.443836447539006196 ) ) ;
#21484=CARTESIAN_POINT ( 'NONE',  ( -84.55620429048340725, -24.64965694238574656, 8.947790433994198267 ) ) ;
#21485=CARTESIAN_POINT ( 'NONE',  ( 18.95625057990686813, 10.65820999021175730, -1.500000000000002220 ) ) ;
#21487=CARTESIAN_POINT ( 'NONE',  ( -22.22805510923732086, 2.117028069546627922, 11.49999999999999645 ) ) ;
#21490=LINE ( 'NONE', #97630, #8045 ) ;
#21493=ORIENTED_EDGE ( 'NONE', *, *, #9576, .T. ) ;
#21494=ORIENTED_EDGE ( 'NONE', *, *, #70406, .F. ) ;
#21500=DIRECTION ( 'NONE',  ( 0.000000000000000000, 0.9999999999976377785, 2.173523156925979128E-06 ) ) ;
#21502=DIRECTION ( 'NONE',  ( 0.4109113463207474393, 0.000000000000000000, -0.9116753070391184766 ) ) ;
#21505=CARTESIAN_POINT ( 'NONE',  ( -19.35591191756920892, -0.7100623379298715010, -1.500000000000002220 ) ) ;
#21506=DIRECTION ( 'NONE',  ( 3.773278334444167608E-23, -1.000000000000000000, 0.000000000000000000 ) ) ;
#21507=ORIENTED_EDGE ( 'NONE', *, *, #41645, .F. ) ;
#21508=CARTESIAN_POINT ( 'NONE',  ( -8.858824863812619910, -17.32749669425128047, 11.49999999999999645 ) ) ;
#21511=ORIENTED_EDGE ( 'NONE', *, *, #9217, .F. ) ;
#21515=LINE ( 'NONE', #83421, #94140 ) ;
#21517=CARTESIAN_POINT ( 'NONE',  ( 18.19143915067776263, 7.407926943018095400, -1.500000000000002220 ) ) ;
#21518=B_SPLINE_SURFACE_WITH_KNOTS ( 'NONE', 3, 1, ( 
 ( #41498, #74798 ),
 ( #26267, #59598 ),
 ( #18642, #49620 ),
 ( #11044, #42009 ),
 ( #72951, #3448 ),
 ( #15392, #84414 ),
 ( #77284, #30621 ),
 ( #38731, #84907 ),
 ( #16392, #91524 ),
 ( #47359, #45373 ),
 ( #6293, #68701 ),
 ( #69697, #53980 ),
 ( #23490, #62093 ),
 ( #6784, #179 ),
 ( #76290, #99129 ),
 ( #7786, #62587 ),
 ( #85407, #100108 ),
 ( #52979, #83915 ),
 ( #61602, #37741 ),
 ( #675, #31120 ),
 ( #93013, #24008 ),
 ( #14393, #46354 ),
 ( #54471, #99620 ),
 ( #92518, #30121 ),
 ( #29628, #15894 ),
 ( #61094, #22992 ),
 ( #37251, #22496 ) ),
 .UNSPECIFIED., .F., .F., .F.,
 ( 4, 1, 1, 1, 1, 1, 1, 1, 1, 1, 1, 1, 1, 1, 1, 1, 1, 1, 1, 1, 1, 1, 1, 1, 4 ),
 ( 2, 2 ),
 ( 0.000000000000000000, 0.04401447057613983027, 0.08743412366770532407, 0.1301183986578977048, 0.1725536945581823134, 0.2145547559681394989, 0.2562980920971315024, 0.2984382251332498015, 0.3408490025880946961, 0.3827151889670263873, 0.4239240454075315911, 0.4642462432504168568, 0.5040736714617970460, 0.5438619058684905916, 0.5835667249796533396, 0.6230943188523323517, 0.6632290607685835671, 0.7035512586114681666, 0.7439378946861853192, 0.7845412548000912922, 0.8257501112405982724, 0.8677573633885087290, 0.9107451640323117603, 0.9549144468914786410, 1.000000000000000000 ),
 ( 0.000000000000000000, 1.000000000000000000 ),
 .UNSPECIFIED. ) ;
#21519=FACE_OUTER_BOUND ( 'NONE', #9732, .T. ) ;
#21521=CARTESIAN_POINT ( 'NONE',  ( 17.62533924669398999, -12.40915598911231577, 11.49999999999998934 ) ) ;
#21524=CARTESIAN_POINT ( 'NONE',  ( -50.52287095715006160, -24.14321612903118108, -0.2833117244520885203 ) ) ;
#21525=CARTESIAN_POINT ( 'NONE',  ( -99.67151487672813914, -25.18439404741721788, 3.611381302008842997 ) ) ;
#21526=CARTESIAN_POINT ( 'NONE',  ( 22.18053613645642841, 6.281410551025238043, -1.500000000000002220 ) ) ;
#21530=LINE ( 'NONE', #67743, #79858 ) ;
#21531=CARTESIAN_POINT ( 'NONE',  ( 5.670567493371958534, -19.34269084982597775, 11.49999999999999645 ) ) ;
#21535=DIRECTION ( 'NONE',  ( -3.773278334453079618E-23, 0.9999999999976377785, 2.173523156925979975E-06 ) ) ;
#21536=CARTESIAN_POINT ( 'NONE',  ( -111.1810695982967161, -25.29779247168320566, 3.716321001747168395 ) ) ;
#21537=CARTESIAN_POINT ( 'NONE',  ( 15.94990109002195489, -11.90149544800030590, -1.500000000000002220 ) ) ;
#21539=DIRECTION ( 'NONE',  ( 0.000000000000000000, 2.173523156925980399E-06, -0.9999999999976378895 ) ) ;
#21540=CARTESIAN_POINT ( 'NONE',  ( 19.48663422773152121, -3.193742178437300794, -1.500000000000002220 ) ) ;
#21541=LINE ( 'NONE', #14434, #81576 ) ;
#21545=CARTESIAN_POINT ( 'NONE',  ( -125.6228709571500275, -23.84081130438200802, 10.88220057463249191 ) ) ;
#21547=CARTESIAN_POINT ( 'NONE',  ( 10.45329875151443488, -17.81600612866554556, 11.49999999999999645 ) ) ;
#21548=CARTESIAN_POINT ( 'NONE',  ( -128.5895376238167103, -24.64965694238408034, 8.947790433994645909 ) ) ;
#21549=CARTESIAN_POINT ( 'NONE',  ( -97.52287095715006160, -24.64965694238575011, 8.947790433994194714 ) ) ;
#21551=CARTESIAN_POINT ( 'NONE',  ( -106.6344508903434019, -23.48783264082477729, -1.443836473390085695 ) ) ;
#21552=CARTESIAN_POINT ( 'NONE',  ( -4.086358941109507370, -22.34742993483353146, 11.49999999999999645 ) ) ;
#21556=CARTESIAN_POINT ( 'NONE',  ( 0.4983251850863967269, 20.17815531296474418, -1.500000000000002220 ) ) ;
#21557=CARTESIAN_POINT ( 'NONE',  ( -115.6228709571500559, -29.50250243563736774, 8.947779886222134493 ) ) ;
#21558=CARTESIAN_POINT ( 'NONE',  ( -52.52287095715006870, -24.64965694238574656, 8.947790433994203596 ) ) ;
#21561=VERTEX_POINT ( 'NONE', #10373 ) ;
#21563=CARTESIAN_POINT ( 'NONE',  ( 19.82229641098322404, 11.46754112681587046, -1.500000000000002220 ) ) ;
#21564=CARTESIAN_POINT ( 'NONE',  ( -29.53721135371585760, -24.26652312753709140, 0.1864212292069160337 ) ) ;
#21565=CARTESIAN_POINT ( 'NONE',  ( -14.38888013576714719, -16.06800976983558726, -1.500000000000002220 ) ) ;
#21566=FACE_OUTER_BOUND ( 'NONE', #77739, .T. ) ;
#21567=CARTESIAN_POINT ( 'NONE',  ( -127.6234793054417338, -24.66019654487200441, 8.947790411086106843 ) ) ;
#21569=CARTESIAN_POINT ( 'NONE',  ( 11.28189403632909915, 17.58240144430209995, 11.49999999999999645 ) ) ;
#21570=ORIENTED_EDGE ( 'NONE', *, *, #12213, .T. ) ;
#21571=CARTESIAN_POINT ( 'NONE',  ( -69.87926231432713564, -25.24754257055753115, 4.903253054825144730 ) ) ;
#21572=CARTESIAN_POINT ( 'NONE',  ( 5.346615758220810477, 21.33151429383102382, -1.500000000000002220 ) ) ;
#21574=CARTESIAN_POINT ( 'NONE',  ( -28.74184145762639631, -24.79700204495068760, 7.085838617364061065 ) ) ;
#21576=VERTEX_POINT ( 'NONE', #26608 ) ;
#21578=CARTESIAN_POINT ( 'NONE',  ( -96.62287095715005592, -24.64965695001468404, 8.947790433994178727 ) ) ;
#21580=CARTESIAN_POINT ( 'NONE',  ( -72.56475950965167954, -23.48786465467241058, 11.44779295918254824 ) ) ;
#21582=AXIS2_PLACEMENT_3D ( 'NONE', #7540, #92765, #23251 ) ;
#21585=CARTESIAN_POINT ( 'NONE',  ( -71.63071712269331215, -24.35071581493543391, 9.817618358456021710 ) ) ;
#21587=CARTESIAN_POINT ( 'NONE',  ( -57.50308292730503723, -24.15543982623907127, -0.2315651400026663420 ) ) ;
#21588=CARTESIAN_POINT ( 'NONE',  ( 18.16468007720714795, -9.286844270591712913, -1.500000000000002220 ) ) ;
#21591=CARTESIAN_POINT ( 'NONE',  ( -99.52287095715009002, -24.66019654487200441, 8.947790411086119278 ) ) ;
#21592=CARTESIAN_POINT ( 'NONE',  ( -97.52287095715006160, -29.50247984919015209, -1.443849546365050029 ) ) ;
#21593=CARTESIAN_POINT ( 'NONE',  ( -91.52287095715009002, -23.72747288104470087, -1.053458166803225904 ) ) ;
#21596=CARTESIAN_POINT ( 'NONE',  ( -28.90723246652128609, -24.63645969467739150, 7.813650128146762519 ) ) ;
#21597=B_SPLINE_CURVE_WITH_KNOTS ( 'NONE', 3,
 ( #35931, #37928, #7972, #23689, #868, #100296 ),
 .UNSPECIFIED., .F., .F.,
 ( 4, 2, 4 ),
 ( 0.000000000000000000, 0.001380764517854763014, 0.002761529035709526028 ),
 .UNSPECIFIED. ) ;
#21598=CARTESIAN_POINT ( 'NONE',  ( 15.20108283357335921, -14.20388156210760577, -1.500000000000002220 ) ) ;
#21602=ORIENTED_EDGE ( 'NONE', *, *, #61490, .F. ) ;
#21603=B_SPLINE_CURVE_WITH_KNOTS ( 'NONE', 3,
 ( #7220, #64441, #30565, #79624 ),
 .UNSPECIFIED., .F., .F.,
 ( 4, 4 ),
 ( 0.000000000000000000, 9.999999999998897304E-05 ),
 .UNSPECIFIED. ) ;
#21604=B_SPLINE_SURFACE_WITH_KNOTS ( 'NONE', 3, 1, ( 
 ( #65706, #71300 ),
 ( #18004, #95633 ),
 ( #48467, #49976 ),
 ( #80903, #2295 ),
 ( #33733, #26624 ),
 ( #40345, #1786 ),
 ( #32725, #96137 ),
 ( #79896, #63708 ),
 ( #65213, #94624 ),
 ( #10389, #73301 ),
 ( #41347, #79397 ),
 ( #57585, #64715 ),
 ( #9887, #72300 ),
 ( #25105, #33225 ),
 ( #3795, #64206 ) ),
 .UNSPECIFIED., .F., .F., .F.,
 ( 4, 1, 1, 1, 1, 1, 1, 1, 1, 1, 1, 1, 4 ),
 ( 2, 2 ),
 ( 0.000000000000000000, 0.08594794314412776415, 0.1691252118806905458, 0.2503991071860499074, 0.3322897361388365001, 0.4133642879158791472, 0.4941722833711859053, 0.5760217353866371459, 0.6607569692540058437, 0.7457831259137418511, 0.8300435929752247866, 0.9140275458206815751, 1.000000000000000000 ),
 ( 0.000000000000000000, 1.000000000000000000 ),
 .UNSPECIFIED. ) ;
#21605=CARTESIAN_POINT ( 'NONE',  ( -98.62287095715005592, -23.48783264082478439, -1.443836473390061936 ) ) ;
#21606=ORIENTED_EDGE ( 'NONE', *, *, #33610, .T. ) ;
#21607=ORIENTED_EDGE ( 'NONE', *, *, #72131, .T. ) ;
#21609=CARTESIAN_POINT ( 'NONE',  ( -55.52287095715005449, -23.48783264082477018, -1.443836473390094577 ) ) ;
#21610=DIRECTION ( 'NONE',  ( -3.773278334453079030E-23, 0.9999999999976377785, 2.173523156925979128E-06 ) ) ;
#21611=CARTESIAN_POINT ( 'NONE',  ( -105.6228709571500559, -29.50248528299804818, 1.056150453629043584 ) ) ;
#21612=CARTESIAN_POINT ( 'NONE',  ( 6.025212951983072607, -21.27585971943098642, 11.49999999999999645 ) ) ;
#21615=CARTESIAN_POINT ( 'NONE',  ( -72.62287095715004170, -23.73907113216991860, -1.053371485793228146 ) ) ;
#21617=CARTESIAN_POINT ( 'NONE',  ( -20.48750165597241590, 9.616757810196778777, -1.500000000000002220 ) ) ;
#21618=CARTESIAN_POINT ( 'NONE',  ( -124.5228709571500616, -23.47593901973090524, -1.443836447538996204 ) ) ;
#21619=VERTEX_POINT ( 'NONE', #75751 ) ;
#21620=B_SPLINE_CURVE_WITH_KNOTS ( 'NONE', 3,
 ( #90316, #7074, #53263, #52261 ),
 .UNSPECIFIED., .F., .F.,
 ( 4, 4 ),
 ( 0.000000000000000000, 9.999999999998897304E-05 ),
 .UNSPECIFIED. ) ;
#21624=CARTESIAN_POINT ( 'NONE',  ( -15.79248070760165490, 12.47733877207048181, 11.49999999999998934 ) ) ;
#21626=ORIENTED_EDGE ( 'NONE', *, *, #66305, .T. ) ;
#21628=CARTESIAN_POINT ( 'NONE',  ( 13.15158565771796084, -18.08388448789661851, -1.500000000000002220 ) ) ;
#21629=EDGE_LOOP ( 'NONE', ( #92238, #88940, #65850, #60272 ) ) ;
#21630=VERTEX_POINT ( 'NONE', #12859 ) ;
#21631=DIRECTION ( 'NONE',  ( -3.773278334453079030E-23, 0.9999999999976377785, 2.173523156925979128E-06 ) ) ;
#21632=DIRECTION ( 'NONE',  ( 0.000000000000000000, -0.9999999999976377785, -2.173523156925979128E-06 ) ) ;
#21635=DIRECTION ( 'NONE',  ( 3.773278334444166432E-23, -1.000000000000000000, 0.000000000000000000 ) ) ;
#21636=CARTESIAN_POINT ( 'NONE',  ( 7.694069055508638399, 17.95645395709951941, -1.500000000000002220 ) ) ;
#21638=CARTESIAN_POINT ( 'NONE',  ( -13.16228656746626591, 16.97819584282690286, 11.49999999999998934 ) ) ;
#21640=DIRECTION ( 'NONE',  ( 1.000000000000000000, 3.773278334444166432E-23, 8.201307841325785021E-29 ) ) ;
#21641=CARTESIAN_POINT ( 'NONE',  ( -34.52287095715006160, -24.50216790748203266, 0.6166512839542475088 ) ) ;
#21642=CARTESIAN_POINT ( 'NONE',  ( 20.43669262517703800, -10.12641136740851699, -1.500000000000002220 ) ) ;
#21643=AXIS2_PLACEMENT_3D ( 'NONE', #91300, #76554, #37016 ) ;
#21646=DIRECTION ( 'NONE',  ( -3.773278334453079618E-23, 0.9999999999976377785, 2.173523156925979975E-06 ) ) ;
#21648=CARTESIAN_POINT ( 'NONE',  ( 8.914523860536577970, -17.85282776015759154, 11.49999999999999645 ) ) ;
#21649=DIRECTION ( 'NONE',  ( 1.000000000000000000, 3.773278334444167608E-23, 8.201307833595939069E-29 ) ) ;
#21651=CARTESIAN_POINT ( 'NONE',  ( -39.61746832362916848, -23.48786465467240703, 11.44779295918255002 ) ) ;
#21652=CARTESIAN_POINT ( 'NONE',  ( -108.6228709571500701, -24.33832256526968862, 0.1851278514119918950 ) ) ;
#21653=ORIENTED_EDGE ( 'NONE', *, *, #82442, .T. ) ;
#21655=CARTESIAN_POINT ( 'NONE',  ( -70.58953762381671027, -23.48786465467241058, 11.44779295918254469 ) ) ;
#21656=CARTESIAN_POINT ( 'NONE',  ( -20.31635052000798325, -7.690577546848336610, 11.49999999999998934 ) ) ;
#21657=CARTESIAN_POINT ( 'NONE',  ( -66.52287095715006160, -23.47596703998600631, 11.44779298504228748 ) ) ;
#21658=CARTESIAN_POINT ( 'NONE',  ( -14.21210043416151159, 13.53504130633199765, -1.500000000000002220 ) ) ;
#21659=CARTESIAN_POINT ( 'NONE',  ( -100.4426124108961176, -25.13313949306887451, 7.101635536975466678 ) ) ;
#21660=ORIENTED_EDGE ( 'NONE', *, *, #86831, .F. ) ;
#21664=CARTESIAN_POINT ( 'NONE',  ( 20.39306652673287701, -2.074774109220689500, 11.49999999999999645 ) ) ;
#21666=CARTESIAN_POINT ( 'NONE',  ( -93.55620429048337883, -23.48783264082478084, -1.443836473390063713 ) ) ;
#21669=CARTESIAN_POINT ( 'NONE',  ( -62.52287095715006160, -24.50321055353804311, 9.387540953477525818 ) ) ;
#21673=CARTESIAN_POINT ( 'NONE',  ( -123.5228709571500616, -24.64965694238408034, 8.947790433994191162 ) ) ;
#21675=EDGE_LOOP ( 'NONE', ( #83768, #12504, #88921, #22086 ) ) ;
#21677=ADVANCED_FACE ( 'NONE', ( #45330 ), #12363, .T. ) ;
#21678=EDGE_CURVE ( 'NONE', #75171, #81379, #27610, .T. ) ;
#21679=CARTESIAN_POINT ( 'NONE',  ( -14.75821945985506645, 17.75411527500383002, 11.49999999999999645 ) ) ;
#21680=CARTESIAN_POINT ( 'NONE',  ( -20.44213351528904354, 10.05872170072450977, 11.49999999999998934 ) ) ;
#21681=CARTESIAN_POINT ( 'NONE',  ( -34.22287095715006444, -23.47596703998600276, 11.44779298504227683 ) ) ;
#21683=CARTESIAN_POINT ( 'NONE',  ( -105.6228709571500417, -24.62226745350444546, 0.9660975649729522940 ) ) ;
#21685=ADVANCED_FACE ( 'NONE', ( #74762 ), #68161, .T. ) ;
#21686=CARTESIAN_POINT ( 'NONE',  ( -115.5228709571500474, -24.52232992886360563, 0.6492154411906000400 ) ) ;
#21687=CARTESIAN_POINT ( 'NONE',  ( -99.64934318012689118, -25.30157686769864966, 4.927356324713951352 ) ) ;
#21689=CARTESIAN_POINT ( 'NONE',  ( 21.88901064076550185, 0.7357440816682787599, 11.49999999999998934 ) ) ;
#21691=CARTESIAN_POINT ( 'NONE',  ( -87.54287233632688014, -24.66019654487200441, 8.947790411086112172 ) ) ;
#21692=DIRECTION ( 'NONE',  ( 0.000000000000000000, 0.9999999999976377785, 2.173523156925979128E-06 ) ) ;
#21693=CARTESIAN_POINT ( 'NONE',  ( -125.5562042904833930, -24.99156044556202261, 7.747789690856173195 ) ) ;
#21694=CARTESIAN_POINT ( 'NONE',  ( -61.64687923781919920, -29.50249039766296022, 3.409318347773680369 ) ) ;
#21696=EDGE_LOOP ( 'NONE', ( #21244, #31954, #6149, #28236 ) ) ;
#21697=CARTESIAN_POINT ( 'NONE',  ( 13.86372479123709311, 15.02075200336711092, -1.500000000000002220 ) ) ;
#21698=ORIENTED_EDGE ( 'NONE', *, *, #38540, .F. ) ;
#21699=ORIENTED_EDGE ( 'NONE', *, *, #44468, .T. ) ;
#21700=VERTEX_POINT ( 'NONE', #67179 ) ;
#21701=ORIENTED_EDGE ( 'NONE', *, *, #40871, .T. ) ;
#21702=EDGE_CURVE ( 'NONE', #75490, #38526, #37253, .T. ) ;
#21703=CARTESIAN_POINT ( 'NONE',  ( 17.08057647167376913, 15.47633299359885761, 11.49999999999998934 ) ) ;
#21704=CARTESIAN_POINT ( 'NONE',  ( -35.52287095715006160, -24.63287334234369297, 0.9662140553102194218 ) ) ;
#21705=CARTESIAN_POINT ( 'NONE',  ( -18.67835518149133378, -7.740158416121700746, -1.500000000000002220 ) ) ;
#21706=ORIENTED_EDGE ( 'NONE', *, *, #80237, .F. ) ;
#21707=CARTESIAN_POINT ( 'NONE',  ( -54.62287095715005592, -24.64965695001467694, 8.947790433994185832 ) ) ;
#21708=CARTESIAN_POINT ( 'NONE',  ( -40.49165087243459737, -25.30353303947430987, 5.543942858925161588 ) ) ;
#21709=CARTESIAN_POINT ( 'NONE',  ( -127.9228709571500815, -23.47596703998600631, 11.44779298504227860 ) ) ;
#21710=CARTESIAN_POINT ( 'NONE',  ( -99.58876850471365572, -24.35071581493543391, 9.817618358456025263 ) ) ;
#21711=CARTESIAN_POINT ( 'NONE',  ( 18.57079561221590325, -10.74342183689097574, 11.49999999999999645 ) ) ;
#21713=FACE_OUTER_BOUND ( 'NONE', #38309, .T. ) ;
#21715=VERTEX_POINT ( 'NONE', #97113 ) ;
#21716=CARTESIAN_POINT ( 'NONE',  ( -20.61657899823519813, -2.091364977790679980, 11.49999999999998934 ) ) ;
#21717=EDGE_CURVE ( 'NONE', #38068, #41731, #28104, .T. ) ;
#21720=EDGE_CURVE ( 'NONE', #42461, #55826, #99087, .T. ) ;
#21721=CARTESIAN_POINT ( 'NONE',  ( -28.50260975624814819, -23.79695530739836329, -0.6495505116914124244 ) ) ;
#21722=ORIENTED_EDGE ( 'NONE', *, *, #57736, .T. ) ;
#21724=ORIENTED_EDGE ( 'NONE', *, *, #29482, .T. ) ;
#21725=CARTESIAN_POINT ( 'NONE',  ( 10.18035917307295435, 18.35650967997132099, -1.500000000000002220 ) ) ;
#21726=B_SPLINE_CURVE_WITH_KNOTS ( 'NONE', 3,
 ( #100003, #53867, #59479, #52863, #92407, #77175, #69078, #36631 ),
 .UNSPECIFIED., .F., .F.,
 ( 4, 2, 2, 4 ),
 ( 0.000000000000000000, 0.002001079623178224527, 0.003001619434767338526, 0.004002159246356452524 ),
 .UNSPECIFIED. ) ;
#21727=CARTESIAN_POINT ( 'NONE',  ( -12.87221125579857528, -17.80329210173279364, 11.49999999999999645 ) ) ;
#21728=ADVANCED_FACE ( 'NONE', ( #6747 ), #36709, .T. ) ;
#21729=CARTESIAN_POINT ( 'NONE',  ( -37.57567300276403444, -24.66019654487199730, 8.947790411086113949 ) ) ;
#21730=CARTESIAN_POINT ( 'NONE',  ( 21.27769986149581172, 7.469961712261545372, -1.500000000000002220 ) ) ;
#21731=CARTESIAN_POINT ( 'NONE',  ( -20.39251343623233836, 4.912230638944180328, -1.500000000000002220 ) ) ;
#21732=EDGE_CURVE ( 'NONE', #62904, #59914, #66693, .T. ) ;
#21736=VERTEX_POINT ( 'NONE', #20472 ) ;
#21737=EDGE_CURVE ( 'NONE', #79503, #45193, #58808, .T. ) ;
#21738=ORIENTED_EDGE ( 'NONE', *, *, #37579, .T. ) ;
#21739=ORIENTED_EDGE ( 'NONE', *, *, #20116, .T. ) ;
#21741=VECTOR ( 'NONE', #100136, 1000.000000000000114 ) ;
#21742=CARTESIAN_POINT ( 'NONE',  ( -19.93307770644097232, -8.117153041090405807, -1.500000000000002220 ) ) ;
#21744=VERTEX_POINT ( 'NONE', #20970 ) ;
#21745=CARTESIAN_POINT ( 'NONE',  ( 14.88031740681034698, -14.96734982212533183, 11.49999999999998934 ) ) ;
#21747=LINE ( 'NONE', #45118, #5971 ) ;
#21748=CARTESIAN_POINT ( 'NONE',  ( -35.62287095715005592, -24.99132157543083821, 2.256160258750667502 ) ) ;
#21750=DIRECTION ( 'NONE',  ( -3.773278334453080206E-23, 0.9999999999976377785, 2.173523156925979975E-06 ) ) ;
#21751=CARTESIAN_POINT ( 'NONE',  ( -19.90388773112789167, 9.559999800501117306, -1.500000000000002220 ) ) ;
#21752=LINE ( 'NONE', #67456, #19261 ) ;
#21757=LINE ( 'NONE', #84165, #72809 ) ;
#21758=CARTESIAN_POINT ( 'NONE',  ( -62.52208505296627550, -23.48786465467241058, 11.44779295918255002 ) ) ;
#21759=CARTESIAN_POINT ( 'NONE',  ( -7.499459838998954631, -17.95702976299720532, 11.49999999999998934 ) ) ;
#21760=CARTESIAN_POINT ( 'NONE',  ( -19.64189229742525455, -8.423329616690555355, 11.49999999999998934 ) ) ;
#21761=CARTESIAN_POINT ( 'NONE',  ( -70.16128103861791487, -25.04479545170914179, 7.555221618711828846 ) ) ;
#21764=CARTESIAN_POINT ( 'NONE',  ( -36.62287095715007723, -24.51387760970723662, 9.387446482453421837 ) ) ;
#21765=CARTESIAN_POINT ( 'NONE',  ( -11.86362535333686807, -19.25999739251378173, -1.500000000000002220 ) ) ;
#21766=B_SPLINE_CURVE_WITH_KNOTS ( 'NONE', 3,
 ( #43866, #4806, #51479, #35759 ),
 .UNSPECIFIED., .F., .F.,
 ( 4, 4 ),
 ( 0.5591709285427831633, 0.5601716755835483008 ),
 .UNSPECIFIED. ) ;
#21767=VERTEX_POINT ( 'NONE', #51941 ) ;
#21769=DIRECTION ( 'NONE',  ( 0.8898870177566430284, -9.915199454925210578E-07, 0.4561809899888475961 ) ) ;
#21770=CARTESIAN_POINT ( 'NONE',  ( 6.953341435731974940, 18.52374150113109152, 11.49999999999999645 ) ) ;
#21771=CARTESIAN_POINT ( 'NONE',  ( -76.58953762381673869, -23.48783264082478084, -1.443836473390065489 ) ) ;
#21772=ORIENTED_EDGE ( 'NONE', *, *, #17582, .F. ) ;
#21773=B_SPLINE_CURVE_WITH_KNOTS ( 'NONE', 3,
 ( #85285, #8169, #9673, #56370, #85796, #94403, #94902, #62462 ),
 .UNSPECIFIED., .F., .F.,
 ( 4, 2, 2, 4 ),
 ( -0.001240355328176767288, -0.0002398155169398778330, 0.0007607242942970116224, 0.002761803916770795737 ),
 .UNSPECIFIED. ) ;
#21774=CARTESIAN_POINT ( 'NONE',  ( -66.55620429048340725, -24.64898659630528854, 1.056161002820824368 ) ) ;
#21775=CARTESIAN_POINT ( 'NONE',  ( -115.5228709571500616, -25.00158670708909625, 2.256160236439166411 ) ) ;
#21776=CARTESIAN_POINT ( 'NONE',  ( -0.6006773669993965559, 21.62980403441659760, 11.49999999999998934 ) ) ;
#21778=CARTESIAN_POINT ( 'NONE',  ( 8.513215801882951794, -17.43586836189350819, -1.500000000000002220 ) ) ;
#21780=CARTESIAN_POINT ( 'NONE',  ( -35.62287095715006302, -24.92579138211019085, 1.929029949965666013 ) ) ;
#21781=CARTESIAN_POINT ( 'NONE',  ( 18.46520180437041603, 7.126043738416648843, -1.500000000000002220 ) ) ;
#21782=ORIENTED_EDGE ( 'NONE', *, *, #72066, .F. ) ;
#21783=VECTOR ( 'NONE', #9068, 1000.000000000000114 ) ;
#21784=CARTESIAN_POINT ( 'NONE',  ( 6.844040470191356640, -19.11863935190610064, 11.49999999999999645 ) ) ;
#21786=B_SPLINE_CURVE_WITH_KNOTS ( 'NONE', 3,
 ( #89336, #74597, #5088, #36533, #82709, #36039 ),
 .UNSPECIFIED., .F., .F.,
 ( 4, 2, 4 ),
 ( 1.570755371633993761E-05, 0.001396183895866087753, 0.002776660238015835579 ),
 .UNSPECIFIED. ) ;
#21788=ADVANCED_FACE ( 'NONE', ( #44333 ), #98595, .F. ) ;
#21790=B_SPLINE_SURFACE_WITH_KNOTS ( 'NONE', 3, 3, ( 
 ( #41127, #41632, #72574, #19267 ),
 ( #10670, #94399, #48237, #79168 ),
 ( #11655, #64487, #34009, #25891 ),
 ( #94895, #25387, #80676, #56364 ),
 ( #3564, #87795, #34510, #65482 ),
 ( #88802, #98382, #97882, #27886 ),
 ( #52230, #50735, #36491, #74070 ) ),
 .UNSPECIFIED., .F., .F., .F.,
 ( 4, 3, 4 ),
 ( 4, 4 ),
 ( 0.0004766839783845224225, 0.1029713700210912741, 0.2054660560637980304 ),
 ( 0.1395294911668197024, 0.1406065943737035973 ),
 .UNSPECIFIED. ) ;
#21791=CARTESIAN_POINT ( 'NONE',  ( -102.5909799838791088, -24.15620529776628445, 10.23563542870660292 ) ) ;
#21792=CARTESIAN_POINT ( 'NONE',  ( -63.62287095715004881, -29.50250243563736774, 8.947779886222145151 ) ) ;
#21793=PLANE ( 'NONE',  #71029 ) ;
#21794=EDGE_CURVE ( 'NONE', #97387, #60884, #93982, .T. ) ;
#21796=CARTESIAN_POINT ( 'NONE',  ( -50.47238528336495733, -25.12325454535568880, 7.100110082141690704 ) ) ;
#21797=CARTESIAN_POINT ( 'NONE',  ( -18.39468835979788608, -8.022455445098881199, -1.500000000000002220 ) ) ;
#21798=EDGE_CURVE ( 'NONE', #30073, #31528, #53442, .T. ) ;
#21801=CARTESIAN_POINT ( 'NONE',  ( -72.55620429048340725, -24.64898659630528854, 1.056161002820823036 ) ) ;
#21802=EDGE_CURVE ( 'NONE', #8909, #12190, #44251, .T. ) ;
#21804=CARTESIAN_POINT ( 'NONE',  ( -10.82450569625279613, 20.10975305113172951, 11.49999999999999645 ) ) ;
#21805=CARTESIAN_POINT ( 'NONE',  ( -50.16163650206989644, -25.31297212321189605, 4.712129047060907183 ) ) ;
#21806=CARTESIAN_POINT ( 'NONE',  ( -86.62287095715004170, -24.64898659630528854, 1.056161002820827921 ) ) ;
#21807=CARTESIAN_POINT ( 'NONE',  ( -114.5562042904833788, -24.65952944569305316, 1.056160979905703234 ) ) ;
#21808=EDGE_CURVE ( 'NONE', #76224, #58188, #4362, .T. ) ;
#21812=DIRECTION ( 'NONE',  ( -3.773278334453079030E-23, 0.9999999999976377785, 2.173523156925979128E-06 ) ) ;
#21813=ORIENTED_EDGE ( 'NONE', *, *, #94312, .T. ) ;
#21814=CARTESIAN_POINT ( 'NONE',  ( -20.15914900662387055, -2.930279687489938389, 11.49999999999998934 ) ) ;
#21815=ORIENTED_EDGE ( 'NONE', *, *, #19698, .F. ) ;
#21816=ADVANCED_FACE ( 'NONE', ( #8256 ), #15352, .F. ) ;
#21817=CARTESIAN_POINT ( 'NONE',  ( 7.334040449947802465, -21.76207178258647090, 11.49999999999998934 ) ) ;
#21818=CARTESIAN_POINT ( 'NONE',  ( -37.62287095715006302, -24.65952944569304250, 1.056160979905693020 ) ) ;
#21821=CARTESIAN_POINT ( 'NONE',  ( -108.6278307361934594, -24.15620529776629155, 10.23563542870659404 ) ) ;
#21822=CARTESIAN_POINT ( 'NONE',  ( -77.58471930946036821, -24.51419770103158768, 9.386484678747166299 ) ) ;
#21824=CARTESIAN_POINT ( 'NONE',  ( -51.59326263455098172, -24.15620529776628089, 10.23563542870660470 ) ) ;
#21825=CARTESIAN_POINT ( 'NONE',  ( -3.310264809446246570, -21.00426241492911927, 11.49999999999999645 ) ) ;
#21828=CARTESIAN_POINT ( 'NONE',  ( 20.56832688555235222, -8.368550285707721414, 11.49999999999998934 ) ) ;
#21829=CARTESIAN_POINT ( 'NONE',  ( -18.09956831669839872, 9.893135806712603397, -1.500000000000002220 ) ) ;
#21830=EDGE_CURVE ( 'NONE', #17220, #26478, #69149, .T. ) ;
#21832=ORIENTED_EDGE ( 'NONE', *, *, #19324, .T. ) ;
#21835=VERTEX_POINT ( 'NONE', #76739 ) ;
#21838=B_SPLINE_CURVE_WITH_KNOTS ( 'NONE', 3,
 ( #7008, #30339, #37955, #15117 ),
 .UNSPECIFIED., .F., .F.,
 ( 4, 4 ),
 ( 0.8003574401347743894, 0.8093638714068899231 ),
 .UNSPECIFIED. ) ;
#21839=CARTESIAN_POINT ( 'NONE',  ( -41.53954185366745122, -24.35071581493542681, 9.817618358456032368 ) ) ;
#21840=CARTESIAN_POINT ( 'NONE',  ( -85.52287095715006160, -23.47596703998600631, 11.44779298504228393 ) ) ;
#21841=CARTESIAN_POINT ( 'NONE',  ( -8.262104503270727207, -19.10415460921518971, -1.500000000000002220 ) ) ;
#21842=CARTESIAN_POINT ( 'NONE',  ( -12.31242093702619123, -17.95196869449987531, 11.49999999999999645 ) ) ;
#21843=CARTESIAN_POINT ( 'NONE',  ( -40.52227049441191298, -25.27806139208687597, 5.079412585072950570 ) ) ;
#21844=CARTESIAN_POINT ( 'NONE',  ( -52.52287095715006160, -23.72747288104470087, -1.053458166803227680 ) ) ;
#21845=CARTESIAN_POINT ( 'NONE',  ( 21.16529133594374557, -7.503415950508986576, 11.49999999999998934 ) ) ;
#21846=EDGE_CURVE ( 'NONE', #53793, #31312, #90253, .T. ) ;
#21847=CARTESIAN_POINT ( 'NONE',  ( -50.80769758106637823, -25.26334732355762824, 4.647238457533181766 ) ) ;
#21848=ORIENTED_EDGE ( 'NONE', *, *, #48200, .T. ) ;
#21851=AXIS2_PLACEMENT_3D ( 'NONE', #39895, #93675, #93170 ) ;
#21852=ORIENTED_EDGE ( 'NONE', *, *, #96206, .F. ) ;
#21853=EDGE_LOOP ( 'NONE', ( #58125, #71237, #88153, #56619, #65626, #96766, #64869, #7000, #19436 ) ) ;
#21855=CARTESIAN_POINT ( 'NONE',  ( -46.60716005348672297, -23.73791477778911840, 11.05961554403171299 ) ) ;
#21856=EDGE_LOOP ( 'NONE', ( #70778, #74853 ) ) ;
#21857=CARTESIAN_POINT ( 'NONE',  ( -9.236746577462426444, 19.23066362772381055, -1.500000000000002220 ) ) ;
#21860=CARTESIAN_POINT ( 'NONE',  ( -2.129267666952235682, 20.92775224702969439, -1.500000000000002220 ) ) ;
#21861=DIRECTION ( 'NONE',  ( -0.000000000000000000, 2.173523156925979552E-06, -0.9999999999976378895 ) ) ;
#21862=CARTESIAN_POINT ( 'NONE',  ( -111.2450078774014344, -25.25753193669086016, 3.808477968289406768 ) ) ;
#21863=DIRECTION ( 'NONE',  ( 3.773278334444166432E-23, -1.000000000000000000, 0.000000000000000000 ) ) ;
#21864=CARTESIAN_POINT ( 'NONE',  ( 20.57945552106664877, -7.502658216658728563, -1.500000000000002220 ) ) ;
#21866=ORIENTED_EDGE ( 'NONE', *, *, #54772, .T. ) ;
#21867=CARTESIAN_POINT ( 'NONE',  ( -40.01839366089613748, -25.29500187561385260, 5.509688069775453556 ) ) ;
#21868=CARTESIAN_POINT ( 'NONE',  ( -50.62287095715005592, -29.50249982740957577, 7.747779886224967605 ) ) ;
#21869=B_SPLINE_CURVE_WITH_KNOTS ( 'NONE', 3,
 ( #5554, #98895, #43628, #89301, #50743, #74566, #27896, #81689, #36500, #96909 ),
 .UNSPECIFIED., .F., .F.,
 ( 4, 2, 2, 2, 4 ),
 ( 0.000000000000000000, 0.0004035656830125077606, 0.0008071313660250155212, 0.001210697049037523336, 0.001614262732050031042 ),
 .UNSPECIFIED. ) ;
#21870=CARTESIAN_POINT ( 'NONE',  ( -130.5728709571500588, -23.47596703998600631, 11.44779298504227860 ) ) ;
#21871=CARTESIAN_POINT ( 'NONE',  ( -10.23453989644235484, -23.17878777331894469, 8.640809912072077381 ) ) ;
#21872=CARTESIAN_POINT ( 'NONE',  ( 14.64190796094839264, -15.47823801613018269, -1.500000000000002220 ) ) ;
#21873=CARTESIAN_POINT ( 'NONE',  ( -98.51141593473609248, -24.35071581493543391, 9.817618358456027039 ) ) ;
#21874=CARTESIAN_POINT ( 'NONE',  ( -107.5144641672072794, -24.35071581493543746, 9.817618358456021710 ) ) ;
#21877=CARTESIAN_POINT ( 'NONE',  ( -33.48326937963503269, -24.51314013834315375, 0.6176544820404119562 ) ) ;
#21878=CARTESIAN_POINT ( 'NONE',  ( 21.67916507323446496, -5.852930566066080864, -1.500000000000002220 ) ) ;
#21880=ORIENTED_EDGE ( 'NONE', *, *, #14760, .T. ) ;
#21881=CARTESIAN_POINT ( 'NONE',  ( -81.52287095715004739, -23.96177878511308634, 10.65340807706330395 ) ) ;
#21882=CARTESIAN_POINT ( 'NONE',  ( -19.07250549579359244, -4.594354733287289605, 11.49999999999999645 ) ) ;
#21883=CARTESIAN_POINT ( 'NONE',  ( -96.62287095715005592, -29.50248528299804818, 1.056150453629042030 ) ) ;
#21885=ORIENTED_EDGE ( 'NONE', *, *, #11340, .F. ) ;
#21887=PLANE ( 'NONE',  #60423 ) ;
#21889=FACE_OUTER_BOUND ( 'NONE', #94599, .T. ) ;
#21891=CARTESIAN_POINT ( 'NONE',  ( -26.02232103978952438, -24.75203499431761500, 7.265335466635947093 ) ) ;
#21892=CARTESIAN_POINT ( 'NONE',  ( -16.88869819569221065, 10.18974688345344148, 11.49999999999998934 ) ) ;
#21894=DIRECTION ( 'NONE',  ( 0.000000000000000000, -2.173523156925980399E-06, 0.9999999999976378895 ) ) ;
#21895=CARTESIAN_POINT ( 'NONE',  ( -116.6228709571500701, -23.48783264082478794, -1.443836473390058606 ) ) ;
#21898=ORIENTED_EDGE ( 'NONE', *, *, #63293, .T. ) ;
#21900=CARTESIAN_POINT ( 'NONE',  ( -103.6228709571500559, -24.66019654487199375, 8.947790411086124607 ) ) ;
#21903=DIRECTION ( 'NONE',  ( 0.000000000000000000, -2.173523156925979552E-06, 0.9999999999976378895 ) ) ;
#21904=EDGE_CURVE ( 'NONE', #38251, #20637, #63673, .T. ) ;
#21905=CARTESIAN_POINT ( 'NONE',  ( -69.71577706848860601, -25.24515085459215769, 5.512506713422812510 ) ) ;
#21907=CARTESIAN_POINT ( 'NONE',  ( -107.5552281182121845, -23.96119346886881729, -0.6495511937831858207 ) ) ;
#21908=CARTESIAN_POINT ( 'NONE',  ( 19.63333621495807435, 3.783328549194958867, 11.49999999999998934 ) ) ;
#21909=B_SPLINE_CURVE_WITH_KNOTS ( 'NONE', 3,
 ( #19649, #81566, #59733, #69708 ),
 .UNSPECIFIED., .F., .F.,
 ( 4, 4 ),
 ( 1.387778780781445676E-17, 0.0001000000000000028508 ),
 .UNSPECIFIED. ) ;
#21910=EDGE_CURVE ( 'NONE', #82077, #48068, #91494, .T. ) ;
#21912=LINE ( 'NONE', #39152, #100231 ) ;
#21913=VERTEX_POINT ( 'NONE', #62051 ) ;
#21914=B_SPLINE_CURVE_WITH_KNOTS ( 'NONE', 3,
 ( #73373, #50045, #79477, #3378, #3871, #11466, #34310, #10462, #26193, #9465, #41422, #2874, #65288, #34809 ),
 .UNSPECIFIED., .F., .F.,
 ( 4, 2, 2, 2, 2, 2, 4 ),
 ( 0.000000000000000000, 0.0001605340506961548935, 0.0003210681013923097869, 0.0006421362027846000582, 0.0009632043041768902211, 0.001123738354873028960, 0.001284272405569167590 ),
 .UNSPECIFIED. ) ;
#21917=CARTESIAN_POINT ( 'NONE',  ( -109.5228709571500616, -23.47593901973090524, -1.443836447538996426 ) ) ;
#21919=CARTESIAN_POINT ( 'NONE',  ( -80.62881840819318313, -24.73531770709095312, 8.716586749053508498 ) ) ;
#21921=CARTESIAN_POINT ( 'NONE',  ( -39.53341462708579712, -24.51314013834315730, 0.6176544820404118452 ) ) ;
#21924=CARTESIAN_POINT ( 'NONE',  ( -34.62287095715004881, -23.96127896941631619, -0.6493128931037907003 ) ) ;
#21925=CARTESIAN_POINT ( 'NONE',  ( -70.52287095715007581, -29.50248528299804818, 1.056150453629036701 ) ) ;
#21926=ORIENTED_EDGE ( 'NONE', *, *, #70427, .F. ) ;
#21927=CARTESIAN_POINT ( 'NONE',  ( 0.8729654516333695824, -20.24016528753796962, -1.500000000000002220 ) ) ;
#21928=CARTESIAN_POINT ( 'NONE',  ( -119.5228709571500758, -29.50250243563736774, 8.947779886222134493 ) ) ;
#21929=CARTESIAN_POINT ( 'NONE',  ( -80.48900664166535535, -25.12298712672050982, 7.101635559041870494 ) ) ;
#21930=LINE ( 'NONE', #52913, #46045 ) ;
#21932=DIRECTION ( 'NONE',  ( -3.773278334453079030E-23, 0.9999999999976377785, 2.173523156925979128E-06 ) ) ;
#21934=CARTESIAN_POINT ( 'NONE',  ( 18.99975792849237877, 6.539580213093530325, -1.500000000000002220 ) ) ;
#21935=CARTESIAN_POINT ( 'NONE',  ( -11.11193726737652199, 17.91617163517716804, 11.49999999999999645 ) ) ;
#21936=CARTESIAN_POINT ( 'NONE',  ( -101.5228709571500758, -24.64898659630368627, 1.056161002820829697 ) ) ;
#21937=CARTESIAN_POINT ( 'NONE',  ( -22.05048665130746954, -1.834114841651104832, 11.49999999999998934 ) ) ;
#21938=CARTESIAN_POINT ( 'NONE',  ( 12.93548710985481698, 15.95582723538240266, 11.49999999999998934 ) ) ;
#21946=CARTESIAN_POINT ( 'NONE',  ( -67.62287095715004170, -24.50321055353805377, 9.387540953477529371 ) ) ;
#21947=ORIENTED_EDGE ( 'NONE', *, *, #27772, .T. ) ;
#21949=ORIENTED_EDGE ( 'NONE', *, *, #50224, .T. ) ;
#21950=DIRECTION ( 'NONE',  ( -3.773278334444167608E-23, 1.000000000000000000, 0.000000000000000000 ) ) ;
#21951=CARTESIAN_POINT ( 'NONE',  ( -49.36949249605027745, -25.10037777829114702, 7.227091855933934994 ) ) ;
#21952=CARTESIAN_POINT ( 'NONE',  ( -89.62287095714999907, -24.51283580621364777, 0.6167428607019738163 ) ) ;
#21953=CARTESIAN_POINT ( 'NONE',  ( -19.87711886888390822, 5.503898473480427711, -1.500000000000002220 ) ) ;
#21954=B_SPLINE_CURVE_WITH_KNOTS ( 'NONE', 3,
 ( #87203, #41041, #71997, #18683 ),
 .UNSPECIFIED., .F., .F.,
 ( 4, 4 ),
 ( 0.1888945234595363343, 0.1898952705003016106 ),
 .UNSPECIFIED. ) ;
#21956=CARTESIAN_POINT ( 'NONE',  ( -11.65619939812097527, 18.16556634249905855, 11.49999999999999645 ) ) ;
#21957=ORIENTED_EDGE ( 'NONE', *, *, #97587, .F. ) ;
#21959=EDGE_CURVE ( 'NONE', #12627, #33110, #17647, .T. ) ;
#21961=CARTESIAN_POINT ( 'NONE',  ( 16.41691039316204481, 15.16158741987741365, -1.500000000000002220 ) ) ;
#21963=CARTESIAN_POINT ( 'NONE',  ( -79.95270946814521551, -25.12205784548233822, 6.976216635617262796 ) ) ;
#21966=CARTESIAN_POINT ( 'NONE',  ( -50.58953762381672448, -25.00182538069145011, 7.747789668545099317 ) ) ;
#21967=CARTESIAN_POINT ( 'NONE',  ( -49.49482000239348878, -24.35071581493542325, 9.817618358456035921 ) ) ;
#21968=CARTESIAN_POINT ( 'NONE',  ( -18.00717387566553995, 10.56535500573724740, -1.500000000000002220 ) ) ;
#21969=ORIENTED_EDGE ( 'NONE', *, *, #57672, .T. ) ;
#21970=EDGE_CURVE ( 'NONE', #1888, #2927, #64949, .T. ) ;
#21971=CARTESIAN_POINT ( 'NONE',  ( -86.51786579561228052, -23.73766607897671221, -1.055555164236433141 ) ) ;
#21973=ORIENTED_EDGE ( 'NONE', *, *, #27446, .T. ) ;
#21974=CARTESIAN_POINT ( 'NONE',  ( -109.5183300406462479, -23.96169478059713498, 10.65365249895717703 ) ) ;
#21975=CARTESIAN_POINT ( 'NONE',  ( 0.3207198112191017025, -21.10926996749724083, -1.500000000000002220 ) ) ;
#21976=EDGE_CURVE ( 'NONE', #31671, #56351, #99928, .T. ) ;
#21977=EDGE_LOOP ( 'NONE', ( #39301, #28529, #88524, #78616 ) ) ;
#21978=FACE_OUTER_BOUND ( 'NONE', #56166, .T. ) ;
#21979=CARTESIAN_POINT ( 'NONE',  ( -99.97649549088345111, -25.26221303177835154, 7.032284653420170173 ) ) ;
#21980=CARTESIAN_POINT ( 'NONE',  ( -16.40380107638378604, 14.33077157581830008, -1.500000000000002220 ) ) ;
#21983=CARTESIAN_POINT ( 'NONE',  ( -79.48403147916279465, -25.21891630973060572, 6.539601158515170987 ) ) ;
#21984=CARTESIAN_POINT ( 'NONE',  ( -12.31242093702619123, -17.95196869449987531, -1.500000000000002220 ) ) ;
#21985=CARTESIAN_POINT ( 'NONE',  ( -71.70689869863497279, -25.31639743646335816, 6.146638256948438794 ) ) ;
#21986=CARTESIAN_POINT ( 'NONE',  ( 6.212073114426278408, 21.40951068830820958, 11.49999999999999645 ) ) ;
#21988=CARTESIAN_POINT ( 'NONE',  ( -124.4728709571500360, -29.48149383318413896, 5.000941583504025623 ) ) ;
#21989=CARTESIAN_POINT ( 'NONE',  ( -85.53826411963355270, -25.00182538069147142, 7.747789668545045139 ) ) ;
#21990=CARTESIAN_POINT ( 'NONE',  ( -43.62287095715007013, -23.94994826722515668, -0.6494450866351720864 ) ) ;
#21992=VERTEX_POINT ( 'NONE', #56451 ) ;
#21993=B_SPLINE_CURVE_WITH_KNOTS ( 'NONE', 3,
 ( #2575, #72589, #80688, #43133 ),
 .UNSPECIFIED., .F., .F.,
 ( 4, 4 ),
 ( 0.000000000000000000, 9.999999999998897304E-05 ),
 .UNSPECIFIED. ) ;
#21994=ORIENTED_EDGE ( 'NONE', *, *, #11170, .F. ) ;
#21995=CARTESIAN_POINT ( 'NONE',  ( -85.52287095715006160, -23.48786465467241058, 11.44779295918254292 ) ) ;
#21996=CARTESIAN_POINT ( 'NONE',  ( 13.39648796734645231, 16.42122281929413319, 11.49999999999998934 ) ) ;
#21998=CARTESIAN_POINT ( 'NONE',  ( -130.5728709571500019, -23.86952536761623733, -1.017619990082604398 ) ) ;
#22001=CARTESIAN_POINT ( 'NONE',  ( -19.00951991574052968, 3.723548053296564575, -1.500000000000002220 ) ) ;
#22002=CARTESIAN_POINT ( 'NONE',  ( -40.93435094691191267, -25.25978494880519776, 3.590542803917028181 ) ) ;
#22004=CARTESIAN_POINT ( 'NONE',  ( 17.17441491540288823, 9.109037055621362455, 11.49999999999999645 ) ) ;
#22007=CARTESIAN_POINT ( 'NONE',  ( -41.52287095715006870, -23.48786465467240347, 11.44779295918255180 ) ) ;
#22009=DIRECTION ( 'NONE',  ( -1.000000000000000000, -3.773278334444167608E-23, -8.201307833595939069E-29 ) ) ;
#22010=CARTESIAN_POINT ( 'NONE',  ( -97.25938181864586340, -23.78087380709146359, 10.97511746239721653 ) ) ;
#22012=B_SPLINE_CURVE_WITH_KNOTS ( 'NONE', 3,
 ( #2087, #24895, #24399, #41646 ),
 .UNSPECIFIED., .F., .F.,
 ( 4, 4 ),
 ( 5.551115123125782086E-17, 9.999999999998900014E-05 ),
 .UNSPECIFIED. ) ;
#22013=CARTESIAN_POINT ( 'NONE',  ( 14.10018531369908423, 13.67006465538575277, -1.500000000000002220 ) ) ;
#22015=VERTEX_POINT ( 'NONE', #41725 ) ;
#22016=CARTESIAN_POINT ( 'NONE',  ( 10.28227983848843152, -18.94921665015282031, 11.49999999999998934 ) ) ;
#22017=CARTESIAN_POINT ( 'NONE',  ( -80.51244414166535535, -25.04307398257883577, 7.563174194274490780 ) ) ;
#22018=LINE ( 'NONE', #59122, #80479 ) ;
#22019=CARTESIAN_POINT ( 'NONE',  ( -57.62287095715003460, -24.65952944569304606, 1.056160979905696573 ) ) ;
#22020=CARTESIAN_POINT ( 'NONE',  ( -100.0747864355570158, -25.27473232648502233, 3.344773415373787806 ) ) ;
#22021=CARTESIAN_POINT ( 'NONE',  ( 5.395019145045520048, -22.42585393411717121, -1.500000000000002220 ) ) ;
#22024=CARTESIAN_POINT ( 'NONE',  ( -93.54916376374448816, -24.34968618360934656, 0.1864209137778838343 ) ) ;
#22025=CARTESIAN_POINT ( 'NONE',  ( -83.52287095715006160, -29.50250243563736774, 8.947779886222141599 ) ) ;
#22026=CARTESIAN_POINT ( 'NONE',  ( 13.10547390533899836, 15.29217475743441312, 11.49999999999999645 ) ) ;
#22027=CARTESIAN_POINT ( 'NONE',  ( -109.1652331756773862, -25.28814200412482549, 3.437502494680751752 ) ) ;
#22028=CARTESIAN_POINT ( 'NONE',  ( -32.50391374051680060, -23.96169478059712787, 10.65365249895719124 ) ) ;
#22030=EDGE_CURVE ( 'NONE', #79100, #97847, #50370, .T. ) ;
#22033=CARTESIAN_POINT ( 'NONE',  ( -40.62287095715005592, -23.47593901973091235, -1.443836447539011525 ) ) ;
#22035=CARTESIAN_POINT ( 'NONE',  ( 19.12242951303546334, 5.485007674754557527, 11.49999999999998934 ) ) ;
#22037=EDGE_CURVE ( 'NONE', #47882, #43726, #41931, .T. ) ;
#22038=CARTESIAN_POINT ( 'NONE',  ( -97.62287095715005592, -23.48786465467241058, 11.44779295918254114 ) ) ;
#22039=CARTESIAN_POINT ( 'NONE',  ( -16.86558833231006460, 10.32443627698238409, -1.500000000000002220 ) ) ;
#22040=AXIS2_PLACEMENT_3D ( 'NONE', #50048, #74364, #73378 ) ;
#22041=CARTESIAN_POINT ( 'NONE',  ( -126.5218657896009233, -23.73791477778912551, 11.05961554403169878 ) ) ;
#22045=PLANE ( 'NONE',  #92892 ) ;
#22046=CARTESIAN_POINT ( 'NONE',  ( -18.79711486612840332, 8.613068827758688428, 11.49999999999999645 ) ) ;
#22047=CARTESIAN_POINT ( 'NONE',  ( -111.5895376238167245, -24.64965694238407679, 8.947790433994649462 ) ) ;
#22051=CARTESIAN_POINT ( 'NONE',  ( -20.26579564662877075, -10.28286414166031726, 11.49999999999999645 ) ) ;
#22052=EDGE_LOOP ( 'NONE', ( #44367, #74722, #64350, #51326 ) ) ;
#22055=CARTESIAN_POINT ( 'NONE',  ( 15.40757771627215256, 13.04930689719894765, -1.500000000000002220 ) ) ;
#22057=CARTESIAN_POINT ( 'NONE',  ( -60.62287095715004881, -23.47593901973091235, -1.443836447539007972 ) ) ;
#22058=LINE ( 'NONE', #69751, #15606 ) ;
#22063=CARTESIAN_POINT ( 'NONE',  ( 12.66508800429495629, 19.07499079241581086, 11.49999999999998934 ) ) ;
#22065=CARTESIAN_POINT ( 'NONE',  ( 8.597998336517790108, -19.88058937513707392, -1.500000000000002220 ) ) ;
#22066=PLANE ( 'NONE',  #86851 ) ;
#22067=CARTESIAN_POINT ( 'NONE',  ( -114.6228709571500701, -24.50216790748204687, 0.6166512839542572788 ) ) ;
#22068=CARTESIAN_POINT ( 'NONE',  ( -13.90609606471210391, -15.62508359690603221, 11.49999999999999645 ) ) ;
#22070=CARTESIAN_POINT ( 'NONE',  ( -74.52287095715007581, -24.64965694238408034, 8.947790433994200043 ) ) ;
#22071=CARTESIAN_POINT ( 'NONE',  ( 17.71009474140864981, 13.04663522181963309, 11.49999999999998934 ) ) ;
#22073=CARTESIAN_POINT ( 'NONE',  ( -41.86334916006617135, -25.10926027280345707, 4.024173299727788589 ) ) ;
#22075=CARTESIAN_POINT ( 'NONE',  ( -94.62287095715005592, -23.47596703998600631, 11.44779298504227860 ) ) ;
#22076=CARTESIAN_POINT ( 'NONE',  ( -90.62361247365680583, -25.00182538069147142, 7.747789668545044250 ) ) ;
#22077=ORIENTED_EDGE ( 'NONE', *, *, #84471, .F. ) ;
#22080=ORIENTED_EDGE ( 'NONE', *, *, #23941, .F. ) ;
#22081=FACE_OUTER_BOUND ( 'NONE', #23189, .T. ) ;
#22082=CARTESIAN_POINT ( 'NONE',  ( -95.62287095715004170, -24.52323809116984776, 9.355190652339416602 ) ) ;
#22083=CARTESIAN_POINT ( 'NONE',  ( -36.57019023030961336, -23.48783264082477018, -1.443836473390095909 ) ) ;
#22084=CARTESIAN_POINT ( 'NONE',  ( 19.91419669613914678, 4.404666692190684962, -1.500000000000002220 ) ) ;
#22086=ORIENTED_EDGE ( 'NONE', *, *, #2198, .F. ) ;
#22087=CARTESIAN_POINT ( 'NONE',  ( -93.62287095715005592, -24.64965695001468404, 8.947790433994180503 ) ) ;
#22089=AXIS2_PLACEMENT_3D ( 'NONE', #73360, #9950, #3855 ) ;
#22091=CARTESIAN_POINT ( 'NONE',  ( -98.55620429048337883, -24.65952944569304606, 1.056160979905700792 ) ) ;
#22094=CARTESIAN_POINT ( 'NONE',  ( -49.92287095715005307, -23.47596703998600631, 11.44779298504227683 ) ) ;
#22095=CARTESIAN_POINT ( 'NONE',  ( -29.81175120719462157, -25.26247357602138166, 4.942810953739434687 ) ) ;
#22096=CARTESIAN_POINT ( 'NONE',  ( -8.262104503270727207, -19.10415460921518971, -1.500000000000002220 ) ) ;
#22098=EDGE_CURVE ( 'NONE', #44804, #8909, #40708, .T. ) ;
#22099=CARTESIAN_POINT ( 'NONE',  ( -98.62287095715005592, -24.64965695001469115, 8.947790433994178727 ) ) ;
#22103=EDGE_CURVE ( 'NONE', #77156, #96725, #62402, .T. ) ;
#22107=DIRECTION ( 'NONE',  ( 0.000000000000000000, -0.9999999999976377785, -2.173523156925979128E-06 ) ) ;
#22108=CARTESIAN_POINT ( 'NONE',  ( -92.62287095715001328, -23.96177878511308634, 10.65340807706329862 ) ) ;
#22109=CARTESIAN_POINT ( 'NONE',  ( -76.52287095715010423, -23.72773821059537269, 11.05748984161097503 ) ) ;
#22110=AXIS2_PLACEMENT_3D ( 'NONE', #13358, #75263, #68162 ) ;
#22111=CARTESIAN_POINT ( 'NONE',  ( -40.62287095715006302, -23.85229601348996553, 10.88205029486208808 ) ) ;
#22112=CARTESIAN_POINT ( 'NONE',  ( -109.1226296748707654, -25.22180349218709949, 3.485716899910509259 ) ) ;
#22113=CARTESIAN_POINT ( 'NONE',  ( -73.55620429048342146, -24.66019654487199020, 8.947790411086131712 ) ) ;
#22114=CARTESIAN_POINT ( 'NONE',  ( -2.366842300981895519, -21.98859952056468714, 11.49999999999999645 ) ) ;
#22117=CARTESIAN_POINT ( 'NONE',  ( 21.95517018727266390, 5.574673621280945568, 11.49999999999998934 ) ) ;
#22118=CARTESIAN_POINT ( 'NONE',  ( -111.5228709571500758, -24.66019654487200441, 8.947790411086108620 ) ) ;
#22120=ORIENTED_EDGE ( 'NONE', *, *, #36774, .T. ) ;
#22121=B_SPLINE_CURVE_WITH_KNOTS ( 'NONE', 3,
 ( #559, #99005, #29500, #91399 ),
 .UNSPECIFIED., .F., .F.,
 ( 4, 4 ),
 ( 0.6909934214884121406, 0.6999998527605277854 ),
 .UNSPECIFIED. ) ;
#22124=CARTESIAN_POINT ( 'NONE',  ( 4.949566031639514918, 19.51814346981619863, -1.500000000000002220 ) ) ;
#22126=EDGE_LOOP ( 'NONE', ( #3666, #82468, #52577, #17207 ) ) ;
#22127=CARTESIAN_POINT ( 'NONE',  ( -89.52287095715010423, -23.73934037231756733, 11.05740245334328797 ) ) ;
#22128=CARTESIAN_POINT ( 'NONE',  ( -7.907391756136429528, -20.87048397725295956, -1.500000000000002220 ) ) ;
#22129=ORIENTED_EDGE ( 'NONE', *, *, #56277, .F. ) ;
#22132=CARTESIAN_POINT ( 'NONE',  ( -81.81052289590537896, -25.19653879850945444, 6.629276519863234185 ) ) ;
#22134=VECTOR ( 'NONE', #30334, 1000.000000000000114 ) ;
#22137=CARTESIAN_POINT ( 'NONE',  ( -1.081029368968937421, 19.50181592447522050, 11.49999999999998934 ) ) ;
#22138=CARTESIAN_POINT ( 'NONE',  ( -32.62287095715006302, -23.47596703998600276, 11.44779298504227505 ) ) ;
#22139=CARTESIAN_POINT ( 'NONE',  ( 2.695732861974529104, -21.29187259674557708, 11.49999999999998934 ) ) ;
#22142=DIRECTION ( 'NONE',  ( -3.773278334444166432E-23, 1.000000000000000000, 0.000000000000000000 ) ) ;
#22143=CARTESIAN_POINT ( 'NONE',  ( -122.6228709571500559, -24.65952944569305316, 1.056160979905706343 ) ) ;
#22144=CARTESIAN_POINT ( 'NONE',  ( -21.74799678179195794, 7.114197580472080951, -1.500000000000002220 ) ) ;
#22145=CARTESIAN_POINT ( 'NONE',  ( -106.5177683666152717, -23.96169478059714564, 10.65365249895717170 ) ) ;
#22146=CARTESIAN_POINT ( 'NONE',  ( -29.62287095715004881, -24.57333416927490433, 1.056161302446588124 ) ) ;
#22147=CARTESIAN_POINT ( 'NONE',  ( 13.89251353435424363, -14.32104260081073832, 11.49999999999999645 ) ) ;
#22148=CARTESIAN_POINT ( 'NONE',  ( -89.81226385320384509, -25.06732983082694943, 7.447789526168956620 ) ) ;
#22149=CARTESIAN_POINT ( 'NONE',  ( -74.62679211367564847, -24.51419770103159124, 9.386484678747162747 ) ) ;
#22153=CARTESIAN_POINT ( 'NONE',  ( -106.5228709571500758, -23.47596703998600631, 11.44779298504228038 ) ) ;
#22154=CARTESIAN_POINT ( 'NONE',  ( -65.52287095715001897, -24.63345952396254290, 9.038047939301506517 ) ) ;
#22155=B_SPLINE_CURVE_WITH_KNOTS ( 'NONE', 3,
 ( #31268, #321, #63753, #69333, #85552, #39884, #25152, #48514 ),
 .UNSPECIFIED., .F., .F.,
 ( 4, 2, 2, 4 ),
 ( 0.000000000000000000, 0.002001079623178219757, 0.003001619434767331153, 0.004002159246356442983 ),
 .UNSPECIFIED. ) ;
#22156=CARTESIAN_POINT ( 'NONE',  ( -11.39883337241029793, 18.50525654427185884, 11.49999999999998934 ) ) ;
#22158=CARTESIAN_POINT ( 'NONE',  ( -19.37596289572233488, 2.755671585415585767, -1.500000000000002220 ) ) ;
#22159=AXIS2_PLACEMENT_3D ( 'NONE', #56393, #87314, #89322 ) ;
#22160=DIRECTION ( 'NONE',  ( 0.000000000000000000, 0.9999999999976377785, 2.173523156925979975E-06 ) ) ;
#22161=ORIENTED_EDGE ( 'NONE', *, *, #92479, .F. ) ;
#22164=DIRECTION ( 'NONE',  ( 1.000000000000000000, 3.773278334444167608E-23, 8.201307833595939069E-29 ) ) ;
#22165=CARTESIAN_POINT ( 'NONE',  ( -88.52287095715006160, -29.50248528299804818, 1.056150453629040253 ) ) ;
#22166=CARTESIAN_POINT ( 'NONE',  ( -12.04554601739387998, 16.56303510970703385, 11.49999999999999645 ) ) ;
#22167=CARTESIAN_POINT ( 'NONE',  ( -94.52287095715007581, -23.72747288104470087, -1.053458166803226126 ) ) ;
#22169=AXIS2_PLACEMENT_3D ( 'NONE', #63290, #86602, #22684 ) ;
#22173=CARTESIAN_POINT ( 'NONE',  ( -39.61224275064198963, -25.28892508652457849, 3.692191117659460176 ) ) ;
#22177=EDGE_CURVE ( 'NONE', #95349, #72422, #68050, .T. ) ;
#22179=CARTESIAN_POINT ( 'NONE',  ( -42.62287095715006302, -24.50321055353803956, 9.387540953477536476 ) ) ;
#22180=CARTESIAN_POINT ( 'NONE',  ( 11.60186680256600233, 19.91347440808847935, 11.49999999999999645 ) ) ;
#22181=CARTESIAN_POINT ( 'NONE',  ( 20.42703387425654427, 10.12935691860780985, -1.500000000000002220 ) ) ;
#22184=CARTESIAN_POINT ( 'NONE',  ( -60.85008373276800597, -25.19805002435821706, 6.796443416052955655 ) ) ;
#22185=DIRECTION ( 'NONE',  ( -3.773278334444166432E-23, 1.000000000000000000, 0.000000000000000000 ) ) ;
#22186=CARTESIAN_POINT ( 'NONE',  ( -110.5481100400817098, -25.00158670708910336, 2.256160236439219258 ) ) ;
#22187=CARTESIAN_POINT ( 'NONE',  ( 1.548332177993611225, -21.85883989728069565, 11.49999999999998934 ) ) ;
#22188=CARTESIAN_POINT ( 'NONE',  ( -54.58953762381672448, -23.48783264082478084, -1.443836473390070596 ) ) ;
#22189=CARTESIAN_POINT ( 'NONE',  ( -50.62287095715004881, -23.85196035786901092, -0.8779234886474973631 ) ) ;
#22190=CARTESIAN_POINT ( 'NONE',  ( -40.54449484207607668, -25.31535585427448609, 5.077976992978702420 ) ) ;
#22191=CARTESIAN_POINT ( 'NONE',  ( -48.87574965546946260, -25.24455176971168413, 6.222157127945766142 ) ) ;
#22192=CARTESIAN_POINT ( 'NONE',  ( -103.6228709571500417, -24.65952944569304606, 1.056160979905701680 ) ) ;
#22193=CARTESIAN_POINT ( 'NONE',  ( -122.6228709571500843, -23.96177878511309345, 10.65340807706328441 ) ) ;
#22194=ORIENTED_EDGE ( 'NONE', *, *, #43528, .T. ) ;
#22195=CARTESIAN_POINT ( 'NONE',  ( 7.241121213506172438, 19.11196469071355963, 11.49999999999998934 ) ) ;
#22196=ORIENTED_EDGE ( 'NONE', *, *, #53688, .F. ) ;
#22197=ORIENTED_EDGE ( 'NONE', *, *, #4149, .T. ) ;
#22198=ORIENTED_EDGE ( 'NONE', *, *, #3715, .T. ) ;
#22199=VERTEX_POINT ( 'NONE', #4650 ) ;
#22200=EDGE_CURVE ( 'NONE', #70837, #14471, #67261, .T. ) ;
#22201=CARTESIAN_POINT ( 'NONE',  ( -8.497478458550677516, -21.44862750780143656, -1.500000000000002220 ) ) ;
#22202=CARTESIAN_POINT ( 'NONE',  ( -61.63716700260808068, -24.15543982623907127, -0.2315651400026656481 ) ) ;
#22203=CARTESIAN_POINT ( 'NONE',  ( -20.14672940031187665, -1.731937678239350298, -1.500000000000002220 ) ) ;
#22204=ORIENTED_EDGE ( 'NONE', *, *, #74187, .T. ) ;
#22206=CARTESIAN_POINT ( 'NONE',  ( -27.14027225143419741, -25.03511874060541587, 4.027978703335532096 ) ) ;
#22207=CARTESIAN_POINT ( 'NONE',  ( -72.52287095715007581, -23.48786465467241058, 11.44779295918254647 ) ) ;
#22208=EDGE_CURVE ( 'NONE', #82121, #65481, #81805, .T. ) ;
#22210=CARTESIAN_POINT ( 'NONE',  ( -99.51645779387621360, -23.96169478059713853, 10.65365249895717703 ) ) ;
#22211=CARTESIAN_POINT ( 'NONE',  ( -18.57871158907727249, 10.67946855401146777, 11.49999999999999645 ) ) ;
#22213=CARTESIAN_POINT ( 'NONE',  ( -128.6228709571500701, -24.33832256526968862, 0.1851278514119945040 ) ) ;
#22214=DIRECTION ( 'NONE',  ( -3.773278334453080206E-23, 0.9999999999976377785, 2.173523156925979975E-06 ) ) ;
#22215=ORIENTED_EDGE ( 'NONE', *, *, #55584, .T. ) ;
#22217=CARTESIAN_POINT ( 'NONE',  ( -20.61657899823519813, -2.091364977790679980, -1.500000000000002220 ) ) ;
#22220=ORIENTED_EDGE ( 'NONE', *, *, #62098, .T. ) ;
#22222=B_SPLINE_SURFACE_WITH_KNOTS ( 'NONE', 3, 3, ( 
 ( #56723, #33866, #5905, #13010 ),
 ( #58215, #59713, #4425, #98246 ),
 ( #89156, #4920, #67827, #83522 ),
 ( #20627, #6413, #44983, #19630 ),
 ( #51594, #58703, #36863, #43976 ),
 ( #36365, #35864, #68312, #97757 ),
 ( #43486, #37369, #28248, #50592 ) ),
 .UNSPECIFIED., .F., .F., .F.,
 ( 4, 3, 4 ),
 ( 4, 4 ),
 ( 0.0004766839783844792713, 0.1029713700210910104, 0.2054660560637975308 ),
 ( 0.2195498469782498629, 0.2206638714302722182 ),
 .UNSPECIFIED. ) ;
#22223=CARTESIAN_POINT ( 'NONE',  ( -29.55620429048338593, -24.57942546158513508, 8.947790451450490679 ) ) ;
#22226=CARTESIAN_POINT ( 'NONE',  ( 20.57779966680088890, -7.652443150423321683, 11.49999999999999645 ) ) ;
#22227=CARTESIAN_POINT ( 'NONE',  ( -73.56460842735368999, -23.48786465467241058, 11.44779295918254824 ) ) ;
#22228=CARTESIAN_POINT ( 'NONE',  ( 14.20245820080859289, -17.52920931871068433, -1.500000000000002220 ) ) ;
#22229=CARTESIAN_POINT ( 'NONE',  ( 10.18035917307295435, 18.35650967997132099, 11.49999999999998934 ) ) ;
#22232=EDGE_LOOP ( 'NONE', ( #64561, #77272, #9991, #24575 ) ) ;
#22233=ORIENTED_EDGE ( 'NONE', *, *, #89177, .T. ) ;
#22234=VERTEX_POINT ( 'NONE', #20348 ) ;
#22235=CARTESIAN_POINT ( 'NONE',  ( -66.49653113318395015, -24.51314013834316441, 0.6176544820404136216 ) ) ;
#22236=AXIS2_PLACEMENT_3D ( 'NONE', #98338, #21215, #83114 ) ;
#22238=CARTESIAN_POINT ( 'NONE',  ( 20.54099941694853726, 6.510794959084822864, -1.500000000000002220 ) ) ;
#22240=ORIENTED_EDGE ( 'NONE', *, *, #1924, .T. ) ;
#22241=CARTESIAN_POINT ( 'NONE',  ( -7.596101150008887082, -19.70107428960382734, 11.49999999999998934 ) ) ;
#22243=CARTESIAN_POINT ( 'NONE',  ( -56.62287095715005592, -29.50250786944525672, 11.44777988621623876 ) ) ;
#22244=EDGE_CURVE ( 'NONE', #2429, #29553, #35802, .T. ) ;
#22245=CARTESIAN_POINT ( 'NONE',  ( -83.62625791794420138, -24.51419770103157347, 9.386484678747182286 ) ) ;
#22248=FACE_OUTER_BOUND ( 'NONE', #60598, .T. ) ;
#22249=CARTESIAN_POINT ( 'NONE',  ( 2.574831182292884435, -22.01391258260016315, -1.500000000000002220 ) ) ;
#22250=CARTESIAN_POINT ( 'NONE',  ( -71.51122638652783792, -23.96119346886880308, -0.6495511937832095795 ) ) ;
#22252=CARTESIAN_POINT ( 'NONE',  ( -51.08169923747086472, -25.24859996806887708, 4.960538017754059226 ) ) ;
#22253=CARTESIAN_POINT ( 'NONE',  ( -79.62287095715002749, -23.72747288104469376, -1.053458166803226348 ) ) ;
#22255=EDGE_CURVE ( 'NONE', #57335, #31312, #43219, .T. ) ;
#22258=CARTESIAN_POINT ( 'NONE',  ( -18.83898130102433299, -4.906684326670742280, -1.500000000000002220 ) ) ;
#22259=CARTESIAN_POINT ( 'NONE',  ( 16.24497012180664868, 13.92215130028523973, -1.500000000000002220 ) ) ;
#22260=CARTESIAN_POINT ( 'NONE',  ( -62.52208516091440060, -23.48783264082476308, -1.443836473390090580 ) ) ;
#22264=CARTESIAN_POINT ( 'NONE',  ( -15.33504971967173702, 16.71734053393862496, -1.500000000000002220 ) ) ;
#22268=CARTESIAN_POINT ( 'NONE',  ( -19.37706247964952411, -4.161318200553020041, 11.49999999999999645 ) ) ;
#22270=EDGE_CURVE ( 'NONE', #48580, #89004, #39387, .T. ) ;
#22273=CARTESIAN_POINT ( 'NONE',  ( -68.52287095715006160, -23.48783264082476308, -1.443836473390092356 ) ) ;
#22274=CARTESIAN_POINT ( 'NONE',  ( 19.28387207504633949, -9.851753786812027514, -1.500000000000002220 ) ) ;
#22276=CARTESIAN_POINT ( 'NONE',  ( -49.47157371846719087, -25.27517952430710579, 3.177618491393788602 ) ) ;
#22277=CARTESIAN_POINT ( 'NONE',  ( -16.98888496755095545, 9.415225082695979353, -1.500000000000002220 ) ) ;
#22278=CARTESIAN_POINT ( 'NONE',  ( -61.62287095715007013, -23.96127896941632685, -0.6493128931037863705 ) ) ;
#22279=DIRECTION ( 'NONE',  ( 0.000000000000000000, 2.173523156925980399E-06, -0.9999999999976378895 ) ) ;
#22280=CARTESIAN_POINT ( 'NONE',  ( 19.51516567812286596, -3.327523070855789911, -1.500000000000002220 ) ) ;
#22281=ORIENTED_EDGE ( 'NONE', *, *, #68571, .T. ) ;
#22283=CARTESIAN_POINT ( 'NONE',  ( -19.38859340154505873, -6.080128201517944753, 11.49999999999999645 ) ) ;
#22284=CARTESIAN_POINT ( 'NONE',  ( -80.59164251549320568, -24.40034930558991277, 0.3402023900116063482 ) ) ;
#22285=EDGE_CURVE ( 'NONE', #50179, #90405, #46764, .T. ) ;
#22286=DIRECTION ( 'NONE',  ( 3.773278334444166432E-23, -1.000000000000000000, 0.000000000000000000 ) ) ;
#22287=EDGE_CURVE ( 'NONE', #2927, #12184, #85380, .T. ) ;
#22289=CARTESIAN_POINT ( 'NONE',  ( -102.5529375350971719, -24.15620529776628800, 10.23563542870660292 ) ) ;
#22290=CARTESIAN_POINT ( 'NONE',  ( -119.4728709571500502, -25.40675428744130215, 5.000950437788803882 ) ) ;
#22291=CARTESIAN_POINT ( 'NONE',  ( -49.74369414166532977, -25.25214427568299413, 4.940878066772249610 ) ) ;
#22292=CARTESIAN_POINT ( 'NONE',  ( -128.6228709571500417, -24.65952944569305316, 1.056160979905707897 ) ) ;
#22294=CARTESIAN_POINT ( 'NONE',  ( -16.07871291144651593, -12.00523380332558965, -1.500000000000002220 ) ) ;
#22295=B_SPLINE_CURVE_WITH_KNOTS ( 'NONE', 3,
 ( #52930, #60052, #82368, #12352 ),
 .UNSPECIFIED., .F., .F.,
 ( 4, 4 ),
 ( 1.859750800284052969E-05, 0.003138001591829818297 ),
 .UNSPECIFIED. ) ;
#22297=CARTESIAN_POINT ( 'NONE',  ( -85.52287095715009002, -24.62226745350443480, 0.9660975649729474091 ) ) ;
#22299=CARTESIAN_POINT ( 'NONE',  ( -72.62287095715005592, -24.64965695001468404, 8.947790433994184056 ) ) ;
#22302=B_SPLINE_CURVE_WITH_KNOTS ( 'NONE', 3,
 ( #91422, #90437, #6196, #67123 ),
 .UNSPECIFIED., .F., .F.,
 ( 4, 4 ),
 ( 0.000000000000000000, 0.0001000000000000167422 ),
 .UNSPECIFIED. ) ;
#22303=CARTESIAN_POINT ( 'NONE',  ( -22.87863416751641310, 0.2071024363326711970, 11.49999999999999645 ) ) ;
#22304=CARTESIAN_POINT ( 'NONE',  ( -22.17926634000774655, 4.976981427743210951, 11.49999999999998934 ) ) ;
#22305=CARTESIAN_POINT ( 'NONE',  ( -30.47287095715005734, -24.75009217604366896, 1.389584765085777107 ) ) ;
#22306=CARTESIAN_POINT ( 'NONE',  ( -51.22287095715006444, -23.47596703998600631, 11.44779298504227683 ) ) ;
#22307=CARTESIAN_POINT ( 'NONE',  ( -40.33261254874832247, -25.19566596169548589, 3.298413478895628970 ) ) ;
#22308=CARTESIAN_POINT ( 'NONE',  ( -89.52287095715006160, -23.47593901973090169, -1.443836447538996426 ) ) ;
#22309=VECTOR ( 'NONE', #83872, 1000.000000000000114 ) ;
#22314=CARTESIAN_POINT ( 'NONE',  ( -20.10423522397153562, 3.301153050299447056, 11.49999999999998934 ) ) ;
#22316=CARTESIAN_POINT ( 'NONE',  ( 17.43399715339889511, -14.94103553264482720, -1.500000000000002220 ) ) ;
#22317=CARTESIAN_POINT ( 'NONE',  ( -115.5228709571500616, -23.48786465467241769, 11.44779295918253759 ) ) ;
#22318=ORIENTED_EDGE ( 'NONE', *, *, #77692, .T. ) ;
#22319=CARTESIAN_POINT ( 'NONE',  ( -108.5164728378366448, -24.15620529776629510, 10.23563542870659404 ) ) ;
#22323=CARTESIAN_POINT ( 'NONE',  ( -20.90244970016518877, -3.954922567530639199, 11.49999999999999645 ) ) ;
#22325=EDGE_LOOP ( 'NONE', ( #91599, #28955, #98330, #51461 ) ) ;
#22326=CARTESIAN_POINT ( 'NONE',  ( 7.537409830304743430, 20.87355781386819942, 11.49999999999998934 ) ) ;
#22327=CARTESIAN_POINT ( 'NONE',  ( -11.86786554430972096, -16.85652113839894639, -1.500000000000002220 ) ) ;
#22328=ORIENTED_EDGE ( 'NONE', *, *, #28255, .T. ) ;
#22331=CARTESIAN_POINT ( 'NONE',  ( -113.6228709571500417, -24.66019654487199730, 8.947790411086121054 ) ) ;
#22332=ORIENTED_EDGE ( 'NONE', *, *, #7163, .T. ) ;
#22333=CARTESIAN_POINT ( 'NONE',  ( -91.58605177063969904, -24.51314013834316086, 0.6176544820404156200 ) ) ;
#22334=VERTEX_POINT ( 'NONE', #76631 ) ;
#22335=CARTESIAN_POINT ( 'NONE',  ( -125.5801323110720347, -25.21753527833458719, 3.539999278834446539 ) ) ;
#22336=CARTESIAN_POINT ( 'NONE',  ( -88.62287095715004170, -29.50250786944525672, 11.44777988621623344 ) ) ;
#22337=CARTESIAN_POINT ( 'NONE',  ( 20.84756458399398937, 0.1950554047328266483, -1.500000000000002220 ) ) ;
#22338=CARTESIAN_POINT ( 'NONE',  ( -16.08361747308824263, -14.67194924222005170, 11.49999999999999645 ) ) ;
#22339=LINE ( 'NONE', #12737, #33167 ) ;
#22340=CARTESIAN_POINT ( 'NONE',  ( -78.63772173417845579, -23.96169478059713498, 10.65365249895717881 ) ) ;
#22341=CARTESIAN_POINT ( 'NONE',  ( 22.29217321540274099, 2.676729263222305644, -1.500000000000002220 ) ) ;
#22344=CARTESIAN_POINT ( 'NONE',  ( -58.52287095715006160, -24.65952944569304250, 1.056160979905695463 ) ) ;
#22346=B_SPLINE_SURFACE_WITH_KNOTS ( 'NONE', 3, 1, ( 
 ( #27286, #58729 ),
 ( #89679, #27777 ),
 ( #34898, #64880 ),
 ( #89184, #57747 ),
 ( #42023, #72968 ),
 ( #20650, #3460 ),
 ( #20154, #80069 ),
 ( #51119, #65871 ),
 ( #82063, #50619 ),
 ( #41512, #95790 ),
 ( #34396, #65374 ),
 ( #81571, #12547 ),
 ( #96790, #26782 ),
 ( #88687, #19157 ),
 ( #12045, #73958 ),
 ( #30767, #60241 ),
 ( #91168, #37885 ),
 ( #98771, #98268 ),
 ( #29271, #6933 ),
 ( #75933, #90671 ),
 ( #29772, #100250 ),
 ( #45013, #68838 ),
 ( #22635, #36386 ),
 ( #53627, #51622 ),
 ( #99274, #92160 ),
 ( #44505, #52612 ),
 ( #84054, #7425 ) ),
 .UNSPECIFIED., .F., .F., .F.,
 ( 4, 1, 1, 1, 1, 1, 1, 1, 1, 1, 1, 1, 1, 1, 1, 1, 1, 1, 1, 1, 1, 1, 1, 1, 4 ),
 ( 2, 2 ),
 ( 0.000000000000000000, 0.03378811616271054641, 0.06719393237387928652, 0.09986241085682445728, 0.1325666121262581154, 0.1651511732547866207, 0.1979131873557913035, 0.2313190035669617506, 0.2650832782673736010, 0.2992553087581147908, 0.3343985665049780120, 0.3699428235093075723, 0.4062835607000604976, 0.4440638196985086106, 0.4829977068727752676, 0.5233544466133043249, 0.5655365896041486540, 0.6096129240658192394, 0.6563908113764169716, 0.7058854949364569142, 0.7583245002617309272, 0.8138317829411497728, 0.8727945590393895170, 0.9347222295400736680, 1.000000000000000000 ),
 ( 0.000000000000000000, 1.000000000000000000 ),
 .UNSPECIFIED. ) ;
#22348=ORIENTED_EDGE ( 'NONE', *, *, #74378, .T. ) ;
#22349=DIRECTION ( 'NONE',  ( -3.773278334444166432E-23, 1.000000000000000000, 0.000000000000000000 ) ) ;
#22352=CARTESIAN_POINT ( 'NONE',  ( 21.01207135711032237, 3.775690236426352264, -1.500000000000002220 ) ) ;
#22354=CARTESIAN_POINT ( 'NONE',  ( -17.93810645791062441, 10.97360191750010827, -1.500000000000002220 ) ) ;
#22355=CARTESIAN_POINT ( 'NONE',  ( -30.53646390802392929, -24.83533449111644842, 1.633466014234818076 ) ) ;
#22357=CARTESIAN_POINT ( 'NONE',  ( -65.52287095715004739, -24.82576562948885979, 8.398263436605498455 ) ) ;
#22358=CARTESIAN_POINT ( 'NONE',  ( -21.51515180086577317, 4.489188270810763548, -1.500000000000002220 ) ) ;
#22359=CARTESIAN_POINT ( 'NONE',  ( -87.60282549588966106, -23.48783264082478084, -1.443836473390063713 ) ) ;
#22361=CARTESIAN_POINT ( 'NONE',  ( -74.62287095715005592, -24.64965695001467694, 8.947790433994184056 ) ) ;
#22362=ADVANCED_FACE ( 'NONE', ( #91869 ), #12669, .T. ) ;
#22366=CARTESIAN_POINT ( 'NONE',  ( -116.6228709571500133, -24.50216790748204332, 0.6166512839542576119 ) ) ;
#22367=CARTESIAN_POINT ( 'NONE',  ( -39.55620429048340014, -23.48783264082477729, -1.443836473390071484 ) ) ;
#22368=EDGE_CURVE ( 'NONE', #30073, #57610, #69766, .T. ) ;
#22369=CARTESIAN_POINT ( 'NONE',  ( -20.44301536939603992, -23.48238912038987536, 9.960784317162937995 ) ) ;
#22370=B_SPLINE_CURVE_WITH_KNOTS ( 'NONE', 3,
 ( #59035, #89973, #12834, #90964, #51918, #37675 ),
 .UNSPECIFIED., .F., .F.,
 ( 4, 2, 4 ),
 ( 0.000000000000000000, 0.001380901958385393966, 0.002761803916770787931 ),
 .UNSPECIFIED. ) ;
#22371=CARTESIAN_POINT ( 'NONE',  ( 18.63368790978032763, -10.32677859091227113, -1.500000000000002220 ) ) ;
#22372=CARTESIAN_POINT ( 'NONE',  ( -98.55492552392462358, -23.96169478059713498, 10.65365249895717881 ) ) ;
#22373=CARTESIAN_POINT ( 'NONE',  ( -107.5862535881878870, -24.66019654487200441, 8.947790411086112172 ) ) ;
#22376=CARTESIAN_POINT ( 'NONE',  ( -33.58058290153915237, -24.51314013834315375, 0.6176544820404119562 ) ) ;
#22377=CARTESIAN_POINT ( 'NONE',  ( -17.89120377161202313, 13.61666483413312712, -1.500000000000002220 ) ) ;
#22378=CARTESIAN_POINT ( 'NONE',  ( -110.9402950654992708, -25.21970293610405633, 6.713732480141158199 ) ) ;
#22379=ORIENTED_EDGE ( 'NONE', *, *, #37769, .T. ) ;
#22380=B_SPLINE_CURVE_WITH_KNOTS ( 'NONE', 3,
 ( #42374, #20005, #74296, #66714 ),
 .UNSPECIFIED., .F., .F.,
 ( 4, 4 ),
 ( 0.000000000000000000, 0.0001000000000000028644 ),
 .UNSPECIFIED. ) ;
#22381=LINE ( 'NONE', #58118, #6093 ) ;
#22382=CARTESIAN_POINT ( 'NONE',  ( -5.058734511472819051, -18.94576116945722788, 11.49999999999999645 ) ) ;
#22383=DIRECTION ( 'NONE',  ( -3.773278334453079618E-23, 0.9999999999976377785, 2.173523156925979975E-06 ) ) ;
#22385=LINE ( 'NONE', #13283, #83616 ) ;
#22386=ADVANCED_FACE ( 'NONE', ( #10644 ), #87771, .F. ) ;
#22387=EDGE_LOOP ( 'NONE', ( #47995, #28737, #15115, #90187 ) ) ;
#22388=CARTESIAN_POINT ( 'NONE',  ( -88.55141012998306849, -24.15620529776628800, 10.23563542870660115 ) ) ;
#22389=CARTESIAN_POINT ( 'NONE',  ( -125.0509062400423659, -25.34771247321013732, 6.200312561216485108 ) ) ;
#22390=CARTESIAN_POINT ( 'NONE',  ( -89.90249562519868221, -25.22174524493127734, 6.695141717414601068 ) ) ;
#22392=CARTESIAN_POINT ( 'NONE',  ( -19.50520112914412252, -2.896358124273927359, 11.49999999999998934 ) ) ;
#22395=ORIENTED_EDGE ( 'NONE', *, *, #92034, .F. ) ;
#22396=CARTESIAN_POINT ( 'NONE',  ( -120.5228709571501042, -24.63345952396256777, 9.038047939301501188 ) ) ;
#22397=CARTESIAN_POINT ( 'NONE',  ( -118.5228709571501611, -23.96127896941632685, -0.6493128931037936979 ) ) ;
#22401=CARTESIAN_POINT ( 'NONE',  ( -109.6228709571500559, -24.66019654487199730, 8.947790411086124607 ) ) ;
#22406=PLANE ( 'NONE',  #74865 ) ;
#22407=CARTESIAN_POINT ( 'NONE',  ( -91.52287095715007581, -23.72773821059536914, 11.05748984161097326 ) ) ;
#22408=CARTESIAN_POINT ( 'NONE',  ( 12.72590371223024697, 15.41468647733915809, 11.49999999999998934 ) ) ;
#22409=ADVANCED_FACE ( 'NONE', ( #18253 ), #94870, .F. ) ;
#22411=CARTESIAN_POINT ( 'NONE',  ( -45.66178293155309831, -23.85049219812685450, 10.88485053497527133 ) ) ;
#22415=CARTESIAN_POINT ( 'NONE',  ( -80.65304639033715262, -23.48786465467241413, 11.44779295918254824 ) ) ;
#22417=CARTESIAN_POINT ( 'NONE',  ( -81.55436275622071207, -23.96119346886881019, -0.6495511937831893734 ) ) ;
#22420=B_SPLINE_CURVE_WITH_KNOTS ( 'NONE', 3,
 ( #36088, #19359, #6129, #57947 ),
 .UNSPECIFIED., .F., .F.,
 ( 4, 4 ),
 ( 0.000000000000000000, 1.000000000000000000 ),
 .UNSPECIFIED. ) ;
#22421=B_SPLINE_SURFACE_WITH_KNOTS ( 'NONE', 3, 3, ( 
 ( #4826, #66750, #97667, #98653 ),
 ( #29152, #59123, #90059, #82438 ),
 ( #12920, #46882, #16410, #1210 ),
 ( #62115, #85428, #62612, #76308 ),
 ( #23515, #93036, #54490, #70216 ),
 ( #38254, #7810, #15415, #37765 ),
 ( #69213, #38754, #47384, #31643 ),
 ( #92540, #14416, #15914, #24029 ),
 ( #697, #23014, #45393, #22517 ),
 ( #6809, #93533, #8312, #7303 ) ),
 .UNSPECIFIED., .F., .F., .F.,
 ( 4, 3, 3, 4 ),
 ( 4, 4 ),
 ( 0.0004766839783810765570, 0.1491231665100168358, 0.2234464077758347156, 0.2977696490416525954 ),
 ( 0.8996026503961034315, 0.9011514434348439906 ),
 .UNSPECIFIED. ) ;
#22424=VERTEX_POINT ( 'NONE', #95874 ) ;
#22425=CARTESIAN_POINT ( 'NONE',  ( 2.300710779914242110, 20.15441874099239783, -1.500000000000002220 ) ) ;
#22429=CARTESIAN_POINT ( 'NONE',  ( -90.52287095715006160, -23.47593901973090524, -1.443836447538996426 ) ) ;
#22431=ORIENTED_EDGE ( 'NONE', *, *, #94557, .T. ) ;
#22434=CARTESIAN_POINT ( 'NONE',  ( -4.233023369943174075, 19.68221892606961987, -1.500000000000002220 ) ) ;
#22435=CARTESIAN_POINT ( 'NONE',  ( 17.50165659415881336, 11.77592616506222711, 11.49999999999999645 ) ) ;
#22436=DIRECTION ( 'NONE',  ( -3.773278334453079030E-23, 0.9999999999976377785, 2.173523156925979128E-06 ) ) ;
#22437=CARTESIAN_POINT ( 'NONE',  ( 21.00647827173414939, 6.864759178008983831, 11.49999999999998934 ) ) ;
#22438=CARTESIAN_POINT ( 'NONE',  ( 2.947869850540926429, 20.32360706268488215, 11.49999999999998934 ) ) ;
#22439=CARTESIAN_POINT ( 'NONE',  ( -96.52287095715006160, -24.50216790748204332, 0.6166512839542606095 ) ) ;
#22440=CARTESIAN_POINT ( 'NONE',  ( -60.64671536082958880, -24.15503026093916006, -0.2815557561904390993 ) ) ;
#22443=ORIENTED_EDGE ( 'NONE', *, *, #98334, .T. ) ;
#22444=DIRECTION ( 'NONE',  ( -3.773278334453079030E-23, 0.9999999999976377785, 2.173523156925979128E-06 ) ) ;
#22445=CARTESIAN_POINT ( 'NONE',  ( -119.6228709571500559, -29.50250243563736774, 8.947779886222134493 ) ) ;
#22447=ORIENTED_EDGE ( 'NONE', *, *, #80981, .T. ) ;
#22451=CARTESIAN_POINT ( 'NONE',  ( -99.62287095715005592, -23.47596703998600631, 11.44779298504227860 ) ) ;
#22453=CARTESIAN_POINT ( 'NONE',  ( -19.88974639711211623, -5.441847772814488948, -1.500000000000002220 ) ) ;
#22454=CARTESIAN_POINT ( 'NONE',  ( -3.891998276399621481, 21.28400606017829233, 11.49999999999999645 ) ) ;
#22457=CARTESIAN_POINT ( 'NONE',  ( -125.5228709571500616, -23.48786465467241769, 11.44779295918253581 ) ) ;
#22458=CARTESIAN_POINT ( 'NONE',  ( -20.95026660567425481, -7.857139728745305973, -1.500000000000002220 ) ) ;
#22459=CARTESIAN_POINT ( 'NONE',  ( -80.26303174456680267, -25.12205807651210066, 7.082509393110550278 ) ) ;
#22460=CARTESIAN_POINT ( 'NONE',  ( -84.62912479653624587, -24.34968618360934300, 0.1864209137778835568 ) ) ;
#22461=EDGE_LOOP ( 'NONE', ( #54865, #83569, #89895, #40944 ) ) ;
#22463=CARTESIAN_POINT ( 'NONE',  ( -49.65272675066790242, -23.73791477778911840, 11.05961554403170943 ) ) ;
#22464=CARTESIAN_POINT ( 'NONE',  ( -20.92377055399060737, -0.003182555231893603818, -1.500000000000002220 ) ) ;
#22465=EDGE_LOOP ( 'NONE', ( #83910, #75154, #7603, #63955 ) ) ;
#22466=CARTESIAN_POINT ( 'NONE',  ( -67.60280104496969500, -23.73791477778911840, 11.05961554403170766 ) ) ;
#22468=ORIENTED_EDGE ( 'NONE', *, *, #48370, .T. ) ;
#22469=CARTESIAN_POINT ( 'NONE',  ( -128.6228709571500417, -24.33927499327855415, 9.819080762295822495 ) ) ;
#22470=CARTESIAN_POINT ( 'NONE',  ( 20.41123533131232648, 5.719371238976541427, -1.500000000000002220 ) ) ;
#22473=CARTESIAN_POINT ( 'NONE',  ( -99.47310917600722746, -25.26221224442602420, 6.670037606239634265 ) ) ;
#22475=CARTESIAN_POINT ( 'NONE',  ( 21.06710269851327766, -5.618397932909799941, 11.49999999999998934 ) ) ;
#22476=CARTESIAN_POINT ( 'NONE',  ( -96.52287095715006160, -29.50247984919015209, -1.443849546365050029 ) ) ;
#22479=CARTESIAN_POINT ( 'NONE',  ( -79.37867731102689106, -25.25089957557972298, 6.257626200401206873 ) ) ;
#22480=CARTESIAN_POINT ( 'NONE',  ( -16.08361747308824263, -14.67194924222005170, -1.500000000000002220 ) ) ;
#22481=CARTESIAN_POINT ( 'NONE',  ( -71.68214140181162009, -25.31639691930716651, 5.908703739881754124 ) ) ;
#22482=CARTESIAN_POINT ( 'NONE',  ( 2.183928509170398602, -22.20744181112294413, 11.49999999999999645 ) ) ;
#22484=DIRECTION ( 'NONE',  ( 0.000000000000000000, 2.173523156925980399E-06, -0.9999999999976378895 ) ) ;
#22485=DIRECTION ( 'NONE',  ( -3.773278334453079030E-23, 0.9999999999976377785, 2.173523156925979128E-06 ) ) ;
#22487=ORIENTED_EDGE ( 'NONE', *, *, #16919, .T. ) ;
#22488=EDGE_CURVE ( 'NONE', #50699, #60506, #41103, .T. ) ;
#22489=EDGE_CURVE ( 'NONE', #81452, #85746, #33472, .T. ) ;
#22492=ORIENTED_EDGE ( 'NONE', *, *, #51282, .T. ) ;
#22494=CARTESIAN_POINT ( 'NONE',  ( -4.771770383141621608, -20.67029057396967318, 11.49999999999998934 ) ) ;
#22495=PLANE ( 'NONE',  #17414 ) ;
#22496=CARTESIAN_POINT ( 'NONE',  ( -80.51244414166535535, -25.03138299555828894, 7.563174219685121713 ) ) ;
#22497=CARTESIAN_POINT ( 'NONE',  ( -59.58953762381671737, -24.66019654487199375, 8.947790411086138818 ) ) ;
#22499=PLANE ( 'NONE',  #51786 ) ;
#22500=CARTESIAN_POINT ( 'NONE',  ( -45.56057666545407869, -23.85016227208580020, -0.8807180028928389692 ) ) ;
#22503=CARTESIAN_POINT ( 'NONE',  ( 10.09180897563621926, 16.61094848277074476, 11.49999999999999645 ) ) ;
#22504=CARTESIAN_POINT ( 'NONE',  ( -88.88918693012689687, -29.50249691823240994, 6.409318347766594037 ) ) ;
#22507=CARTESIAN_POINT ( 'NONE',  ( -41.52287095715006870, -24.65952944569304606, 1.056160979905691910 ) ) ;
#22508=CARTESIAN_POINT ( 'NONE',  ( -44.58953762381671737, -23.47593901973091235, -1.443836447539011525 ) ) ;
#22511=CARTESIAN_POINT ( 'NONE',  ( -19.07250549579359244, -4.594354733287289605, 11.49999999999998934 ) ) ;
#22513=DIRECTION ( 'NONE',  ( 0.000000000000000000, -0.9999999999976377785, -2.173523156925979128E-06 ) ) ;
#22514=EDGE_LOOP ( 'NONE', ( #28222, #72658, #61819, #67177 ) ) ;
#22515=CARTESIAN_POINT ( 'NONE',  ( 19.30674495121141376, 9.566621930910674365, -1.500000000000002220 ) ) ;
#22516=VECTOR ( 'NONE', #36672, 1000.000000000000114 ) ;
#22517=CARTESIAN_POINT ( 'NONE',  ( -40.47158788874726554, -24.92564183028978775, 1.928384488918254203 ) ) ;
#22518=CARTESIAN_POINT ( 'NONE',  ( -90.52287095715009002, -24.83620972994591725, 8.398175272781365663 ) ) ;
#22519=CARTESIAN_POINT ( 'NONE',  ( -13.44081803467414638, 18.71018530922267686, -1.500000000000002220 ) ) ;
#22522=LINE ( 'NONE', #29656, #19886 ) ;
#22523=CARTESIAN_POINT ( 'NONE',  ( -20.01257119864951051, 2.908879540851186274, 11.49999999999999645 ) ) ;
#22524=FACE_OUTER_BOUND ( 'NONE', #18125, .T. ) ;
#22525=CARTESIAN_POINT ( 'NONE',  ( -91.52287095715006160, -24.65952944569304606, 1.056160979905700570 ) ) ;
#22526=VECTOR ( 'NONE', #81360, 1000.000000000000114 ) ;
#22527=CARTESIAN_POINT ( 'NONE',  ( -110.8797149084312537, -25.10921396279124096, 2.935128329961295357 ) ) ;
#22529=CARTESIAN_POINT ( 'NONE',  ( -110.6372435692922664, -25.29779163436222333, 3.331084253915489235 ) ) ;
#22530=CARTESIAN_POINT ( 'NONE',  ( 18.06118663784855372, 8.336529998961283994, -1.500000000000002220 ) ) ;
#22531=CARTESIAN_POINT ( 'NONE',  ( -97.55620429048339304, -23.48786465467241769, 11.44779295918254114 ) ) ;
#22532=CARTESIAN_POINT ( 'NONE',  ( -19.19514693104756375, 4.742496307885142315, -1.500000000000002220 ) ) ;
#22533=CARTESIAN_POINT ( 'NONE',  ( -56.50282025588294488, -24.15543982623907127, -0.2315651400026670359 ) ) ;
#22535=CARTESIAN_POINT ( 'NONE',  ( -40.37522208020789805, -25.29116519044529099, 2.834757491049489264 ) ) ;
#22536=DIRECTION ( 'NONE',  ( 0.000000000000000000, 0.9999999999976377785, 2.173523156925979128E-06 ) ) ;
#22537=CARTESIAN_POINT ( 'NONE',  ( 7.614520588612671226, -19.20288753073135268, 11.49999999999999645 ) ) ;
#22538=CARTESIAN_POINT ( 'NONE',  ( -98.58953762381672448, -24.64898659630529210, 1.056161002820829475 ) ) ;
#22540=FACE_OUTER_BOUND ( 'NONE', #99593, .T. ) ;
#22542=CARTESIAN_POINT ( 'NONE',  ( -21.73129956901698989, 6.668506094012985663, 11.49999999999999645 ) ) ;
#22544=CARTESIAN_POINT ( 'NONE',  ( -67.52287095715007581, -24.50216790748204687, 0.6166512839542540592 ) ) ;
#22546=CARTESIAN_POINT ( 'NONE',  ( 17.97931717627152182, 9.192180251422895410, 11.49999999999998934 ) ) ;
#22547=CARTESIAN_POINT ( 'NONE',  ( -108.6228709571500417, -23.47596703998600631, 11.44779298504227860 ) ) ;
#22548=LINE ( 'NONE', #13952, #54510 ) ;
#22550=ORIENTED_EDGE ( 'NONE', *, *, #71638, .F. ) ;
#22552=CARTESIAN_POINT ( 'NONE',  ( 21.75204538223844963, -7.182240389990739438, -1.500000000000002220 ) ) ;
#22553=CARTESIAN_POINT ( 'NONE',  ( -51.19827071096799642, -25.18439730688664469, 3.666040128663992981 ) ) ;
#22554=CARTESIAN_POINT ( 'NONE',  ( 2.186256072416925544, -21.55203199515037582, -1.500000000000002220 ) ) ;
#22557=CARTESIAN_POINT ( 'NONE',  ( -12.67655569012464944, 16.65582705476778358, 11.49999999999999645 ) ) ;
#22558=ORIENTED_EDGE ( 'NONE', *, *, #89628, .F. ) ;
#22559=CARTESIAN_POINT ( 'NONE',  ( -69.23586867255411903, -25.24754350588972684, 5.333583042115673578 ) ) ;
#22560=CARTESIAN_POINT ( 'NONE',  ( -0.4018715335629812202, -22.01094342083549193, -1.500000000000002220 ) ) ;
#22562=CARTESIAN_POINT ( 'NONE',  ( -41.32330479122543210, -25.10925829605731607, 3.114706959938358111 ) ) ;
#22564=CARTESIAN_POINT ( 'NONE',  ( -38.62287095715005592, -29.50248528299804818, 1.056150453629031594 ) ) ;
#22565=CARTESIAN_POINT ( 'NONE',  ( -90.58310212721774235, -24.92592662359561473, 8.075495903018000021 ) ) ;
#22567=CARTESIAN_POINT ( 'NONE',  ( -117.6228709571500559, -29.50248528299804818, 1.056150453629045360 ) ) ;
#22571=CARTESIAN_POINT ( 'NONE',  ( -41.58953762381673158, -24.64965694238406613, 8.947790433994661896 ) ) ;
#22572=CARTESIAN_POINT ( 'NONE',  ( -101.7007079832508367, -25.10935996662800562, 3.725872784279629979 ) ) ;
#22573=CARTESIAN_POINT ( 'NONE',  ( -100.5228709571500758, -24.14406661686760103, 10.28769366194082302 ) ) ;
#22574=CARTESIAN_POINT ( 'NONE',  ( 20.14718400222343320, -3.498931157112906476, -1.500000000000002220 ) ) ;
#22575=ORIENTED_EDGE ( 'NONE', *, *, #79700, .T. ) ;
#22578=CARTESIAN_POINT ( 'NONE',  ( -61.52287095715007581, -23.47593901973090169, -1.443836447538997092 ) ) ;
#22579=CARTESIAN_POINT ( 'NONE',  ( -99.52287095715011844, -23.48783264083466449, -1.443836473374706442 ) ) ;
#22580=CARTESIAN_POINT ( 'NONE',  ( -10.38793682863964563, 19.71736701935523683, 11.49999999999998934 ) ) ;
#22581=B_SPLINE_CURVE_WITH_KNOTS ( 'NONE', 3,
 ( #9116, #32457, #24343, #33453, #2024, #10625, #63433, #3024, #94350, #95357, #25842, #8622, #56819, #86741, #17229, #48194, #41587, #9620 ),
 .UNSPECIFIED., .F., .F.,
 ( 4, 2, 2, 2, 2, 2, 2, 2, 4 ),
 ( 0.004711333090593654814, 0.005300261127349137000, 0.005889189164104619185, 0.006478117200860101371, 0.007067045237615584424, 0.007655973274371065743, 0.008244901311126548796, 0.008833829347882030114, 0.009422757384637513167 ),
 .UNSPECIFIED. ) ;
#22583=CARTESIAN_POINT ( 'NONE',  ( -91.52287095715006160, -24.64898659630368272, 1.056161002820827921 ) ) ;
#22585=LINE ( 'NONE', #32212, #16009 ) ;
#22587=CARTESIAN_POINT ( 'NONE',  ( -29.79716636085243664, -25.26247483479900424, 5.521952527462851812 ) ) ;
#22589=CARTESIAN_POINT ( 'NONE',  ( 19.72710162658169608, 6.580912942549038469, -1.500000000000002220 ) ) ;
#22592=VERTEX_POINT ( 'NONE', #85086 ) ;
#22593=VECTOR ( 'NONE', #49359, 1000.000000000000114 ) ;
#22594=CARTESIAN_POINT ( 'NONE',  ( -51.31235188911633571, -25.12217787106197164, 6.754155556777655889 ) ) ;
#22595=ORIENTED_EDGE ( 'NONE', *, *, #16689, .F. ) ;
#22598=CARTESIAN_POINT ( 'NONE',  ( -50.72667573002448904, -25.27412235707870636, 2.869183044873688360 ) ) ;
#22599=EDGE_CURVE ( 'NONE', #47563, #52812, #1837, .T. ) ;
#22602=FACE_OUTER_BOUND ( 'NONE', #63886, .T. ) ;
#22604=CARTESIAN_POINT ( 'NONE',  ( 19.81268554055766273, 9.900562300003143079, 11.49999999999999645 ) ) ;
#22605=EDGE_LOOP ( 'NONE', ( #85865, #45219, #65088, #66500 ) ) ;
#22606=CARTESIAN_POINT ( 'NONE',  ( -105.6228709571500559, -23.47596703998600631, 11.44779298504227860 ) ) ;
#22607=EDGE_CURVE ( 'NONE', #62448, #42265, #51427, .T. ) ;
#22608=CARTESIAN_POINT ( 'NONE',  ( -18.78231125015805958, 12.62931641965373153, 11.49999999999998934 ) ) ;
#22610=CARTESIAN_POINT ( 'NONE',  ( -29.24636659180999843, -25.20264517434234364, 4.940287045316306802 ) ) ;
#22612=B_SPLINE_CURVE_WITH_KNOTS ( 'NONE', 3,
 ( #15840, #48317, #8245, #87364, #48824, #55429, #54924, #40698 ),
 .UNSPECIFIED., .F., .F.,
 ( 4, 2, 2, 4 ),
 ( -0.001240355328176769457, -0.0002398155169398802182, 0.0007607242942970090203, 0.002761803916770789232 ),
 .UNSPECIFIED. ) ;
#22613=ADVANCED_FACE ( 'NONE', ( #76462 ), #99788, .F. ) ;
#22616=PLANE ( 'NONE',  #45050 ) ;
#22617=CARTESIAN_POINT ( 'NONE',  ( -19.68739882612603864, 4.164723872966736629, 11.49999999999998934 ) ) ;
#22618=B_SPLINE_SURFACE_WITH_KNOTS ( 'NONE', 3, 3, ( 
 ( #56536, #33686, #64665, #95578 ),
 ( #87974, #90460, #97572, #12825 ),
 ( #28073, #89962, #20938, #51911 ),
 ( #88976, #13821, #82839, #50413 ),
 ( #81356, #43796, #13320, #75715 ),
 ( #11835, #42808, #59522, #52402 ),
 ( #21427, #44301, #58527, #73739 ) ),
 .UNSPECIFIED., .F., .F., .F.,
 ( 4, 3, 4 ),
 ( 4, 4 ),
 ( 0.0004766839783825378447, 0.1029713700210901917, 0.2054660560637978362 ),
 ( 0.02950150192610306865, 0.03052783842092137920 ),
 .UNSPECIFIED. ) ;
#22619=CARTESIAN_POINT ( 'NONE',  ( -99.58953762381672448, -23.47596703998600631, 11.44779298504227683 ) ) ;
#22622=CARTESIAN_POINT ( 'NONE',  ( 4.697571063781373013, 21.84268702631108994, -1.500000000000002220 ) ) ;
#22623=B_SPLINE_CURVE_WITH_KNOTS ( 'NONE', 3,
 ( #60907, #52285, #91834, #13704 ),
 .UNSPECIFIED., .F., .F.,
 ( 4, 4 ),
 ( 0.009792917360197044008, 0.01879934863231252917 ),
 .UNSPECIFIED. ) ;
#22624=EDGE_CURVE ( 'NONE', #37337, #30827, #31810, .T. ) ;
#22626=EDGE_LOOP ( 'NONE', ( #38026, #22129, #29851, #95485 ) ) ;
#22628=CARTESIAN_POINT ( 'NONE',  ( -80.51244414166535535, -25.03284467579916495, 7.563174216508125269 ) ) ;
#22630=DIRECTION ( 'NONE',  ( -1.000000000000000000, -3.773278334444168195E-23, -8.201307807930740669E-29 ) ) ;
#22632=CARTESIAN_POINT ( 'NONE',  ( 16.94836550497923966, -9.742303593519430649, -1.500000000000002220 ) ) ;
#22634=CARTESIAN_POINT ( 'NONE',  ( -20.40864349294084334, -6.676163967499375573, -1.500000000000002220 ) ) ;
#22635=CARTESIAN_POINT ( 'NONE',  ( -25.56915516548917822, -24.92775208071710935, 4.121106392019679987 ) ) ;
#22636=DIRECTION ( 'NONE',  ( -3.773278334453079030E-23, 0.9999999999976377785, 2.173523156925979128E-06 ) ) ;
#22639=CARTESIAN_POINT ( 'NONE',  ( 18.61037501828884189, -13.27421459584354579, -1.500000000000002220 ) ) ;
#22641=CARTESIAN_POINT ( 'NONE',  ( -94.62287095715005592, -29.50247984919015209, -1.443849546365051806 ) ) ;
#22642=CARTESIAN_POINT ( 'NONE',  ( -60.62287095715004881, -29.50248789122583659, 2.256150453626215580 ) ) ;
#22643=CARTESIAN_POINT ( 'NONE',  ( -19.61284664649099696, 3.773188449817356904, 11.49999999999999645 ) ) ;
#22644=CARTESIAN_POINT ( 'NONE',  ( -60.62287095715004881, -29.50250243563736774, 8.947779886222145151 ) ) ;
#22645=VECTOR ( 'NONE', #84733, 1000.000000000000114 ) ;
#22650=EDGE_CURVE ( 'NONE', #64607, #31523, #19960, .T. ) ;
#22651=CARTESIAN_POINT ( 'NONE',  ( -105.6228709571500559, -23.48786465467241769, 11.44779295918253759 ) ) ;
#22652=CARTESIAN_POINT ( 'NONE',  ( -15.31764660673900558, 15.41647822393392175, 11.49999999999998934 ) ) ;
#22655=CARTESIAN_POINT ( 'NONE',  ( -9.247272915838292917, -17.29429475886123768, -1.500000000000002220 ) ) ;
#22657=VECTOR ( 'NONE', #24961, 1000.000000000000114 ) ;
#22658=CARTESIAN_POINT ( 'NONE',  ( -41.32652706876731230, -25.23761884256712307, 3.713814482909440606 ) ) ;
#22661=CARTESIAN_POINT ( 'NONE',  ( -91.60161349800799258, -23.48786465467241058, 11.44779295918254469 ) ) ;
#22663=CARTESIAN_POINT ( 'NONE',  ( -10.27258457790969892, -17.75692283049141196, 11.49999999999999645 ) ) ;
#22665=CARTESIAN_POINT ( 'NONE',  ( -54.52287095715006870, -23.47596703998600631, 11.44779298504229104 ) ) ;
#22666=B_SPLINE_CURVE_WITH_KNOTS ( 'NONE', 3,
 ( #2403, #81523, #80013, #73413, #20108, #64829 ),
 .UNSPECIFIED., .F., .F.,
 ( 4, 2, 4 ),
 ( 1.570755371634052715E-05, 0.001396183895866087536, 0.002776660238015834278 ),
 .UNSPECIFIED. ) ;
#22668=ORIENTED_EDGE ( 'NONE', *, *, #27010, .F. ) ;
#22669=EDGE_CURVE ( 'NONE', #66017, #53781, #79269, .T. ) ;
#22671=CARTESIAN_POINT ( 'NONE',  ( -39.51912653461286595, -25.18430990892983701, 3.844034515489341608 ) ) ;
#22672=CARTESIAN_POINT ( 'NONE',  ( -125.5222534766403726, -23.48786465467241769, 11.44779295918253581 ) ) ;
#22674=EDGE_CURVE ( 'NONE', #53590, #39121, #52692, .T. ) ;
#22677=CARTESIAN_POINT ( 'NONE',  ( 15.98122378838116120, 16.67787885001082770, 11.49999999999999645 ) ) ;
#22678=CARTESIAN_POINT ( 'NONE',  ( 13.80103769381473811, 18.14473668730428813, -1.500000000000002220 ) ) ;
#22679=CARTESIAN_POINT ( 'NONE',  ( -74.60134285719104241, -23.73766607897670511, -1.055555164236458898 ) ) ;
#22681=CARTESIAN_POINT ( 'NONE',  ( -119.6228709571500559, -24.64898659630368627, 1.056161002820833028 ) ) ;
#22682=CARTESIAN_POINT ( 'NONE',  ( -4.914914792326205983, -21.87198836336805385, 11.49999999999999645 ) ) ;
#22684=DIRECTION ( 'NONE',  ( -3.773278334444166432E-23, 1.000000000000000000, 0.000000000000000000 ) ) ;
#22685=CARTESIAN_POINT ( 'NONE',  ( -21.55542221127511482, -4.010009934288176758, 11.49999999999998934 ) ) ;
#22688=CARTESIAN_POINT ( 'NONE',  ( -87.59490563179548417, -23.96169478059713498, 10.65365249895718058 ) ) ;
#22690=CARTESIAN_POINT ( 'NONE',  ( -78.54013620366454518, -24.65952944569304606, 1.056160979905704789 ) ) ;
#22693=CARTESIAN_POINT ( 'NONE',  ( -16.48689143942861079, 12.14541645011370541, 11.49999999999998934 ) ) ;
#22694=ORIENTED_EDGE ( 'NONE', *, *, #11400, .F. ) ;
#22695=VERTEX_POINT ( 'NONE', #64284 ) ;
#22696=VERTEX_POINT ( 'NONE', #10463 ) ;
#22698=CARTESIAN_POINT ( 'NONE',  ( -10.12245940999746985, -20.73198382670940987, 11.49999999999998934 ) ) ;
#22699=CARTESIAN_POINT ( 'NONE',  ( -61.56641536606631604, -23.48783264082477018, -1.443836473390096575 ) ) ;
#22700=CARTESIAN_POINT ( 'NONE',  ( -14.64122064730360862, 14.02963135428074004, -1.500000000000002220 ) ) ;
#22702=CARTESIAN_POINT ( 'NONE',  ( -29.27791982133463122, -24.88714994053520257, 2.243760839632586102 ) ) ;
#22703=CARTESIAN_POINT ( 'NONE',  ( -41.58770330147535077, -25.31575704012490746, 5.035072416868334066 ) ) ;
#22704=B_SPLINE_CURVE_WITH_KNOTS ( 'NONE', 3,
 ( #82821, #75702, #90938, #44282 ),
 .UNSPECIFIED., .F., .F.,
 ( 4, 4 ),
 ( 0.000000000000000000, 1.000000000000000000 ),
 .UNSPECIFIED. ) ;
#22706=CARTESIAN_POINT ( 'NONE',  ( -70.49786096558409554, -24.52300882791528380, 0.6510814631126248253 ) ) ;
#22707=CARTESIAN_POINT ( 'NONE',  ( -3.722501342491481235, -21.08806747394077519, 11.49999999999999645 ) ) ;
#22709=CARTESIAN_POINT ( 'NONE',  ( -110.5228709571500616, -29.50248528299804818, 1.056150453629043584 ) ) ;
#22710=CARTESIAN_POINT ( 'NONE',  ( -61.61076051278942600, -23.48786465467240703, 11.44779295918255180 ) ) ;
#22712=CARTESIAN_POINT ( 'NONE',  ( -6.500255983836059848, -19.66680810221124887, 11.49999999999998934 ) ) ;
#22713=VECTOR ( 'NONE', #17985, 1000.000000000000114 ) ;
#22714=EDGE_LOOP ( 'NONE', ( #95017, #74696, #8702, #82840 ) ) ;
#22716=ORIENTED_EDGE ( 'NONE', *, *, #77814, .F. ) ;
#22717=CARTESIAN_POINT ( 'NONE',  ( -28.48001184966671673, -24.34880053053494464, 0.6176551810875480220 ) ) ;
#22721=B_SPLINE_CURVE_WITH_KNOTS ( 'NONE', 3,
 ( #72818, #93257, #23744, #24250 ),
 .UNSPECIFIED., .F., .F.,
 ( 4, 4 ),
 ( 0.000000000000000000, 1.000000000000000000 ),
 .UNSPECIFIED. ) ;
#22723=CARTESIAN_POINT ( 'NONE',  ( 12.42595048307055983, -18.10569578304522764, 11.49999999999999645 ) ) ;
#22724=CARTESIAN_POINT ( 'NONE',  ( -89.59156183601115231, -24.15620529776628445, 10.23563542870660115 ) ) ;
#22725=CARTESIAN_POINT ( 'NONE',  ( 22.42242567092132433, 2.420433022335332751, -1.500000000000002220 ) ) ;
#22726=CARTESIAN_POINT ( 'NONE',  ( -19.40599490818632233, 7.965113791304038848, -1.500000000000002220 ) ) ;
#22727=CARTESIAN_POINT ( 'NONE',  ( -48.55620429048338593, -23.48783264082478794, -1.443836473390069708 ) ) ;
#22729=ORIENTED_EDGE ( 'NONE', *, *, #9119, .T. ) ;
#22731=EDGE_CURVE ( 'NONE', #26599, #50012, #9968, .T. ) ;
#22735=EDGE_CURVE ( 'NONE', #27980, #65683, #24820, .T. ) ;
#22736=CARTESIAN_POINT ( 'NONE',  ( -36.62287095715006302, -23.96127896941631619, -0.6493128931037911444 ) ) ;
#22738=CARTESIAN_POINT ( 'NONE',  ( -17.55493245422511350, -12.44833567967518029, -1.500000000000002220 ) ) ;
#22740=CARTESIAN_POINT ( 'NONE',  ( -90.62287095715004170, -24.99156045073392818, 7.747789690856161648 ) ) ;
#22741=ORIENTED_EDGE ( 'NONE', *, *, #75754, .T. ) ;
#22742=CARTESIAN_POINT ( 'NONE',  ( -21.09505027744838657, -1.104435277493458045, 11.49999999999998934 ) ) ;
#22743=PLANE ( 'NONE',  #49810 ) ;
#22744=CARTESIAN_POINT ( 'NONE',  ( -129.6228709571500417, -23.47593901973091235, -1.443836447538995760 ) ) ;
#22745=CARTESIAN_POINT ( 'NONE',  ( -83.58827326063148178, -24.35071581493543036, 9.817618358456028815 ) ) ;
#22746=B_SPLINE_CURVE_WITH_KNOTS ( 'NONE', 3,
 ( #30936, #71517, #62914, #25324, #16210, #71013 ),
 .UNSPECIFIED., .F., .F.,
 ( 4, 2, 4 ),
 ( 6.384118678609748304E-06, 0.001386860460828372816, 0.002767336802978135821 ),
 .UNSPECIFIED. ) ;
#22747=CARTESIAN_POINT ( 'NONE',  ( -33.62287095715005592, -29.50250786944525672, 11.44777988621624409 ) ) ;
#22748=CARTESIAN_POINT ( 'NONE',  ( -99.12737035893434268, -25.25749934748553827, 3.919097026091935110 ) ) ;
#22749=CARTESIAN_POINT ( 'NONE',  ( 21.13975321936677787, -6.629177502137091338, -1.500000000000002220 ) ) ;
#22750=CARTESIAN_POINT ( 'NONE',  ( -71.55916548094597829, -23.73766607897670156, -1.055555164236456012 ) ) ;
#22751=EDGE_CURVE ( 'NONE', #95088, #67931, #61146, .T. ) ;
#22752=VERTEX_POINT ( 'NONE', #78967 ) ;
#22753=CARTESIAN_POINT ( 'NONE',  ( -51.60144572864662393, -25.31633170366855978, 5.335377950845888506 ) ) ;
#22754=CARTESIAN_POINT ( 'NONE',  ( -39.44687923781921057, -25.27828342519987359, 4.188173683033348027 ) ) ;
#22757=CARTESIAN_POINT ( 'NONE',  ( 5.650214204171827070, -18.61605495904187535, -1.500000000000002220 ) ) ;
#22758=CARTESIAN_POINT ( 'NONE',  ( 15.12546962493697933, 15.13007008128210096, -1.500000000000002220 ) ) ;
#22759=CARTESIAN_POINT ( 'NONE',  ( -62.63183165261912677, -24.34968618360933945, 0.1864209137778799485 ) ) ;
#22761=B_SPLINE_CURVE_WITH_KNOTS ( 'NONE', 3,
 ( #51632, #26793, #43026, #50139 ),
 .UNSPECIFIED., .F., .F.,
 ( 4, 4 ),
 ( 0.4590962244662299963, 0.4600969715069954669 ),
 .UNSPECIFIED. ) ;
#22762=CARTESIAN_POINT ( 'NONE',  ( -122.5895376238167387, -24.64965694238408034, 8.947790433994649462 ) ) ;
#22764=CARTESIAN_POINT ( 'NONE',  ( 22.61316900856233403, 2.020702135111208442, -1.500000000000002220 ) ) ;
#22765=FACE_OUTER_BOUND ( 'NONE', #94664, .T. ) ;
#22766=CARTESIAN_POINT ( 'NONE',  ( -57.62287095714999907, -23.96177878511307568, 10.65340807706330573 ) ) ;
#22767=CARTESIAN_POINT ( 'NONE',  ( 18.95923836289803788, 5.684714004613049987, 11.49999999999999645 ) ) ;
#22768=LINE ( 'NONE', #52746, #98245 ) ;
#22772=CARTESIAN_POINT ( 'NONE',  ( 12.90450488963236353, -17.39418326053592168, -1.500000000000002220 ) ) ;
#22774=CARTESIAN_POINT ( 'NONE',  ( -13.34961138979462270, 14.11212085816309880, -1.500000000000002220 ) ) ;
#22775=PLANE ( 'NONE',  #98287 ) ;
#22776=CARTESIAN_POINT ( 'NONE',  ( -35.62287095715005592, -25.00158670708908915, 2.256160236439166855 ) ) ;
#22777=CARTESIAN_POINT ( 'NONE',  ( -12.90690225449951001, 15.05119527412115055, -1.500000000000002220 ) ) ;
#22779=ORIENTED_EDGE ( 'NONE', *, *, #58219, .T. ) ;
#22780=CARTESIAN_POINT ( 'NONE',  ( 20.27773211485958527, -1.686570798567030183, 11.49999999999999645 ) ) ;
#22781=PLANE ( 'NONE',  #52153 ) ;
#22783=EDGE_CURVE ( 'NONE', #5942, #15143, #6667, .T. ) ;
#22786=CARTESIAN_POINT ( 'NONE',  ( -0.09811904274419530614, -21.77977188575789924, -0.5132947483565734048 ) ) ;
#22787=FACE_OUTER_BOUND ( 'NONE', #24767, .T. ) ;
#22788=CARTESIAN_POINT ( 'NONE',  ( -48.87380231474225667, -25.31602077158062869, 6.137091870245725111 ) ) ;
#22789=CARTESIAN_POINT ( 'NONE',  ( -40.56083858672488418, -23.85049219812685095, 10.88485053497527488 ) ) ;
#22790=CARTESIAN_POINT ( 'NONE',  ( -81.62287095715008434, -23.47596703998600631, 11.44779298504227860 ) ) ;
#22791=CARTESIAN_POINT ( 'NONE',  ( -0.1815635828756200498, -20.05798930676971636, 11.49999999999998934 ) ) ;
#22794=B_SPLINE_CURVE_WITH_KNOTS ( 'NONE', 3,
 ( #71260, #18965, #87988, #71766, #3759, #32688, #79860, #64173, #80872, #18465, #1751, #25579, #63669, #49437, #94589, #17972, #10862, #41311, #72270, #2759 ),
 .UNSPECIFIED., .F., .F.,
 ( 4, 2, 2, 2, 2, 2, 2, 2, 2, 4 ),
 ( 0.000000000000000000, 0.0005538341668565423736, 0.001107668333713084747, 0.001661502500569627012, 0.002215336667426169494, 0.002769170834282711977, 0.003323005001139254025, 0.003876839167995796507, 0.004153756251424071434, 0.004430673334852346795 ),
 .UNSPECIFIED. ) ;
#22795=CARTESIAN_POINT ( 'NONE',  ( -30.64427850938830389, -23.56000036390796737, -1.497999999999532594 ) ) ;
#22797=CARTESIAN_POINT ( 'NONE',  ( -1.055347110731411187, -22.84297022578905612, 11.49999999999999645 ) ) ;
#22798=CARTESIAN_POINT ( 'NONE',  ( -22.72798930328562150, -0.2126449523330483371, -1.500000000000002220 ) ) ;
#22801=CARTESIAN_POINT ( 'NONE',  ( -28.52287095715005094, -23.57565896798463356, -1.053490781832481460 ) ) ;
#22802=CARTESIAN_POINT ( 'NONE',  ( -38.52792539663658999, -24.66019654487199375, 8.947790411086119278 ) ) ;
#22803=VECTOR ( 'NONE', #65570, 1000.000000000000114 ) ;
#22804=CARTESIAN_POINT ( 'NONE',  ( -84.52287095715006160, -24.65952944569304606, 1.056160979905698794 ) ) ;
#22808=CARTESIAN_POINT ( 'NONE',  ( -111.5895376238167387, -23.47596703998600631, 11.44779298504227683 ) ) ;
#22809=ORIENTED_EDGE ( 'NONE', *, *, #35767, .F. ) ;
#22810=CARTESIAN_POINT ( 'NONE',  ( 3.729398819442638846, -20.01364129133569136, 11.49999999999998934 ) ) ;
#22811=VERTEX_POINT ( 'NONE', #6985 ) ;
#22812=CARTESIAN_POINT ( 'NONE',  ( -2.116611060711651504, 22.89395876494169002, 11.49999999999998934 ) ) ;
#22813=DIRECTION ( 'NONE',  ( -0.000000000000000000, 2.173523156925979552E-06, -0.9999999999976378895 ) ) ;
#22814=EDGE_CURVE ( 'NONE', #86042, #27009, #84104, .T. ) ;
#22815=EDGE_LOOP ( 'NONE', ( #44700, #43076, #46603, #42936 ) ) ;
#22816=CARTESIAN_POINT ( 'NONE',  ( -101.6228709571500417, -23.72773821059535493, 11.05748984161097681 ) ) ;
#22818=CARTESIAN_POINT ( 'NONE',  ( -40.62287095715004881, -24.91544648472620338, 1.928969306349231028 ) ) ;
#22819=CARTESIAN_POINT ( 'NONE',  ( 1.764508054474889009, 21.21474994468914943, 11.49999999999999645 ) ) ;
#22822=CARTESIAN_POINT ( 'NONE',  ( 9.120982285578694615, 20.23247719416018242, 11.49999999999998934 ) ) ;
#22823=CARTESIAN_POINT ( 'NONE',  ( 4.765357849511589805, 20.07956653139741121, 11.49999999999998934 ) ) ;
#22825=ORIENTED_EDGE ( 'NONE', *, *, #16120, .T. ) ;
#22826=CARTESIAN_POINT ( 'NONE',  ( -109.4178292903974352, -25.31627359254128962, 5.278454429945570681 ) ) ;
#22827=CARTESIAN_POINT ( 'NONE',  ( -39.22520490595655929, -25.22497507903540637, 3.518386540108912719 ) ) ;
#22829=CARTESIAN_POINT ( 'NONE',  ( -91.59147655181246250, -24.15543982623907837, -0.2315651400026614848 ) ) ;
#22830=VERTEX_POINT ( 'NONE', #23195 ) ;
#22831=CARTESIAN_POINT ( 'NONE',  ( -49.52287095715006160, -23.47596703998600631, 11.44779298504229104 ) ) ;
#22834=CARTESIAN_POINT ( 'NONE',  ( -4.186882374726557110, 20.40937146592452223, -1.500000000000002220 ) ) ;
#22835=ADVANCED_FACE ( 'NONE', ( #59791 ), #20769, .T. ) ;
#22836=CARTESIAN_POINT ( 'NONE',  ( 18.38516380405726736, -11.72527425286322611, 11.49999999999999645 ) ) ;
#22839=CARTESIAN_POINT ( 'NONE',  ( -21.66288588771858770, -5.991481186202806342, -1.500000000000002220 ) ) ;
#22840=CARTESIAN_POINT ( 'NONE',  ( -38.66562564847060912, -23.48783264082477729, -1.443836473390076369 ) ) ;
#22841=ORIENTED_EDGE ( 'NONE', *, *, #4947, .T. ) ;
#22842=CARTESIAN_POINT ( 'NONE',  ( -75.62287095715005592, -29.50247984919015209, -1.443849546365053582 ) ) ;
#22843=PLANE ( 'NONE',  #42661 ) ;
#22846=B_SPLINE_CURVE_WITH_KNOTS ( 'NONE', 3,
 ( #96077, #43297, #42314, #81352 ),
 .UNSPECIFIED., .F., .F.,
 ( 4, 4 ),
 ( 0.04982150079182124519, 0.05882793206393686913 ),
 .UNSPECIFIED. ) ;
#22847=VECTOR ( 'NONE', #67730, 1000.000000000000114 ) ;
#22848=EDGE_CURVE ( 'NONE', #65188, #24519, #46583, .T. ) ;
#22850=CARTESIAN_POINT ( 'NONE',  ( -21.15786647118399699, 2.672229404501205163, -1.500000000000002220 ) ) ;
#22852=ORIENTED_EDGE ( 'NONE', *, *, #61193, .T. ) ;
#22853=CARTESIAN_POINT ( 'NONE',  ( -19.96636262075925927, 6.592627302904066511, 11.49999999999998934 ) ) ;
#22854=PLANE ( 'NONE',  #41695 ) ;
#22856=LINE ( 'NONE', #68069, #25555 ) ;
#22857=CARTESIAN_POINT ( 'NONE',  ( -4.682628417673765142, 21.48327871026360114, -1.500000000000002220 ) ) ;
#22860=CARTESIAN_POINT ( 'NONE',  ( -39.22287095715006444, -23.47593901973090524, -1.443836447538998202 ) ) ;
#22862=CARTESIAN_POINT ( 'NONE',  ( -127.6228709571500559, -23.47596703998600631, 11.44779298504227860 ) ) ;
#22866=CARTESIAN_POINT ( 'NONE',  ( -130.5728709571500588, -23.47593901973090524, -1.443836447538995982 ) ) ;
#22867=CARTESIAN_POINT ( 'NONE',  ( -20.45434509553457048, -23.26101209975225004, 10.47594215909544602 ) ) ;
#22868=CARTESIAN_POINT ( 'NONE',  ( 21.27783752795556538, -0.9766432368044721812, 11.49999999999998934 ) ) ;
#22869=CARTESIAN_POINT ( 'NONE',  ( -31.24388727629348494, -24.86181185134534388, 1.747789972853592610 ) ) ;
#22871=CARTESIAN_POINT ( 'NONE',  ( -29.52287095715006160, -23.40102634903646717, 11.44779303447556629 ) ) ;
#22872=CARTESIAN_POINT ( 'NONE',  ( -70.52287095715007581, -23.47593901973090524, -1.443836447538997092 ) ) ;
#22873=CARTESIAN_POINT ( 'NONE',  ( 16.93931825803137414, 14.88162037096512158, -1.500000000000002220 ) ) ;
#22874=CARTESIAN_POINT ( 'NONE',  ( -111.9711312661725913, -25.31476271379807841, 5.144092056987718209 ) ) ;
#22876=CARTESIAN_POINT ( 'NONE',  ( -99.52287095715009002, -23.47593901973090524, -1.443836447538996648 ) ) ;
#22877=CARTESIAN_POINT ( 'NONE',  ( -14.21210043416151159, 13.53504130633199765, 11.49999999999999645 ) ) ;
#22878=CARTESIAN_POINT ( 'NONE',  ( -28.62287095715004170, -24.35949118625558540, 0.6166262265330719750 ) ) ;
#22879=CARTESIAN_POINT ( 'NONE',  ( -82.52287095715001897, -23.48783264083388289, -1.443836473375923690 ) ) ;
#22880=ORIENTED_EDGE ( 'NONE', *, *, #98781, .F. ) ;
#22881=CARTESIAN_POINT ( 'NONE',  ( -88.55459174287842927, -23.96169478059713853, 10.65365249895717703 ) ) ;
#22882=CARTESIAN_POINT ( 'NONE',  ( -124.4728709572981131, -25.40561136979900780, 5.197855858930376272 ) ) ;
#22883=CARTESIAN_POINT ( 'NONE',  ( -91.96540889688385789, -25.22174524493127379, 6.695141717414600180 ) ) ;
#22884=CARTESIAN_POINT ( 'NONE',  ( -6.756748142665309764, -18.51622224137248907, 11.49999999999998934 ) ) ;
#22887=CARTESIAN_POINT ( 'NONE',  ( -69.62287095715005592, -29.50248528299804818, 1.056150453629036701 ) ) ;
#22888=EDGE_CURVE ( 'NONE', #10502, #41620, #99806, .T. ) ;
#22892=CARTESIAN_POINT ( 'NONE',  ( -96.52287095715006160, -24.64898659630528499, 1.056161002820829697 ) ) ;
#22893=CARTESIAN_POINT ( 'NONE',  ( -107.6228709571501128, -24.34917612406838572, 0.1852690917426684236 ) ) ;
#22894=CARTESIAN_POINT ( 'NONE',  ( -29.62287095715004881, -23.40875089534885589, 11.44779299594469713 ) ) ;
#22899=CARTESIAN_POINT ( 'NONE',  ( 10.22567584263966722, 17.17405255344276682, -1.500000000000002220 ) ) ;
#22900=FACE_OUTER_BOUND ( 'NONE', #41366, .T. ) ;
#22901=CARTESIAN_POINT ( 'NONE',  ( -101.5228709571500758, -29.50247984919015209, -1.443849546365050029 ) ) ;
#22902=ORIENTED_EDGE ( 'NONE', *, *, #13587, .T. ) ;
#22904=CARTESIAN_POINT ( 'NONE',  ( -110.0449441895338509, -25.18430161695049918, 3.330200698182170793 ) ) ;
#22905=CARTESIAN_POINT ( 'NONE',  ( -35.67968232430675357, -23.48783264082477729, -1.443836473390077701 ) ) ;
#22908=CARTESIAN_POINT ( 'NONE',  ( -97.62287095715004170, -24.65952944569304606, 1.056160979905701236 ) ) ;
#22910=EDGE_CURVE ( 'NONE', #88368, #21992, #44681, .T. ) ;
#22911=CARTESIAN_POINT ( 'NONE',  ( -61.62287095715004881, -23.47593901973091235, -1.443836447539007972 ) ) ;
#22913=VERTEX_POINT ( 'NONE', #8488 ) ;
#22914=CARTESIAN_POINT ( 'NONE',  ( -16.53579703214142427, -11.71821515807347680, 11.49999999999998934 ) ) ;
#22918=ADVANCED_FACE ( 'NONE', ( #71899 ), #35364, .T. ) ;
#22919=FACE_OUTER_BOUND ( 'NONE', #57447, .T. ) ;
#22920=EDGE_CURVE ( 'NONE', #22830, #17879, #10480, .T. ) ;
#22921=ORIENTED_EDGE ( 'NONE', *, *, #32616, .T. ) ;
#22922=DIRECTION ( 'NONE',  ( 3.773278334444167608E-23, -1.000000000000000000, 0.000000000000000000 ) ) ;
#22923=AXIS2_PLACEMENT_3D ( 'NONE', #88445, #56508, #33146 ) ;
#22924=CARTESIAN_POINT ( 'NONE',  ( 19.84801528777503776, 3.447069022702595742, -1.500000000000002220 ) ) ;
#22925=CARTESIAN_POINT ( 'NONE',  ( 16.02493003730957000, -13.65669227992738577, 11.49999999999999645 ) ) ;
#22927=ADVANCED_FACE ( 'NONE', ( #41441 ), #57218, .T. ) ;
#22928=DIRECTION ( 'NONE',  ( -3.773278334453079618E-23, 0.9999999999976377785, 2.173523156925979975E-06 ) ) ;
#22929=CARTESIAN_POINT ( 'NONE',  ( 20.41560922187292348, 8.460057656491983380, 11.49999999999998934 ) ) ;
#22930=B_SPLINE_CURVE_WITH_KNOTS ( 'NONE', 3,
 ( #23857, #54833, #85768, #16255 ),
 .UNSPECIFIED., .F., .F.,
 ( 4, 4 ),
 ( 0.000000000000000000, 9.999999999998897304E-05 ),
 .UNSPECIFIED. ) ;
#22931=CARTESIAN_POINT ( 'NONE',  ( 20.20254288951482735, -3.758238384022974277, -1.500000000000002220 ) ) ;
#22932=CARTESIAN_POINT ( 'NONE',  ( -98.62287095715011276, -23.73934037231758154, 11.05740245334328975 ) ) ;
#22934=ORIENTED_EDGE ( 'NONE', *, *, #41140, .T. ) ;
#22939=ORIENTED_EDGE ( 'NONE', *, *, #50517, .F. ) ;
#22940=ORIENTED_EDGE ( 'NONE', *, *, #79675, .F. ) ;
#22944=LINE ( 'NONE', #61049, #95769 ) ;
#22945=CARTESIAN_POINT ( 'NONE',  ( 1.647368763193059582, 20.57021071130147405, -1.500000000000002220 ) ) ;
#22948=CARTESIAN_POINT ( 'NONE',  ( 15.64208908530913256, 14.88810259432246852, 11.49999999999999645 ) ) ;
#22950=CARTESIAN_POINT ( 'NONE',  ( -83.62287095715005592, -23.72747288104442021, -1.053458166803661999 ) ) ;
#22952=CARTESIAN_POINT ( 'NONE',  ( -4.763361739610138201, -21.85411462188651299, 11.49999999999998934 ) ) ;
#22953=CARTESIAN_POINT ( 'NONE',  ( -80.45048864170028935, -25.27875090593738960, 7.100579934607695876 ) ) ;
#22954=CARTESIAN_POINT ( 'NONE',  ( -53.52287095715006160, -23.72747288104469732, -1.053458166803227458 ) ) ;
#22956=CARTESIAN_POINT ( 'NONE',  ( -116.6622629653596448, -25.38372066892256740, 5.756446416874773320 ) ) ;
#22957=CARTESIAN_POINT ( 'NONE',  ( -49.56823440250532542, -23.48786465467241058, 11.44779295918254824 ) ) ;
#22958=FACE_OUTER_BOUND ( 'NONE', #85187, .T. ) ;
#22959=CARTESIAN_POINT ( 'NONE',  ( -20.37482282770194075, 4.769447832466558346, 11.49999999999998934 ) ) ;
#22961=CARTESIAN_POINT ( 'NONE',  ( -98.62287095715005592, -23.47593901973091235, -1.443836447539001089 ) ) ;
#22962=ADVANCED_FACE ( 'NONE', ( #20088 ), #10182, .T. ) ;
#22963=ORIENTED_EDGE ( 'NONE', *, *, #85517, .F. ) ;
#22965=DIRECTION ( 'NONE',  ( -1.000000000000000000, -3.773278334444166432E-23, -8.201307841325785021E-29 ) ) ;
#22966=CARTESIAN_POINT ( 'NONE',  ( -7.741094375770895653, -19.69850519626218599, -1.500000000000002220 ) ) ;
#22967=ADVANCED_FACE ( 'NONE', ( #59165 ), #3890, .T. ) ;
#22968=ORIENTED_EDGE ( 'NONE', *, *, #40369, .T. ) ;
#22969=CARTESIAN_POINT ( 'NONE',  ( -117.5545766209327070, -24.15543982623907837, -0.2315651400026547124 ) ) ;
#22971=CARTESIAN_POINT ( 'NONE',  ( -14.02725853290852243, 16.66567569088042688, -1.500000000000002220 ) ) ;
#22972=CARTESIAN_POINT ( 'NONE',  ( -37.62287095715007013, -23.47596703998600276, 11.44779298504227505 ) ) ;
#22973=CARTESIAN_POINT ( 'NONE',  ( -41.52287095715006870, -24.33832256527048088, 0.1851278514138547937 ) ) ;
#22974=CARTESIAN_POINT ( 'NONE',  ( -79.92287095715006728, -23.47593901973090169, -1.443836447538997092 ) ) ;
#22975=CARTESIAN_POINT ( 'NONE',  ( -19.11951126197014261, -10.51958540666066533, -1.500000000000002220 ) ) ;
#22976=CARTESIAN_POINT ( 'NONE',  ( -71.60837349177994327, -25.24674223047061261, 5.637668537290724480 ) ) ;
#22979=CARTESIAN_POINT ( 'NONE',  ( -117.5228709571500758, -23.47593901973090524, -1.443836447538996204 ) ) ;
#22982=ORIENTED_EDGE ( 'NONE', *, *, #65035, .F. ) ;
#22985=EDGE_CURVE ( 'NONE', #80749, #59957, #80980, .T. ) ;
#22986=EDGE_LOOP ( 'NONE', ( #85774, #13608, #55341, #46731 ) ) ;
#22987=B_SPLINE_CURVE_WITH_KNOTS ( 'NONE', 3,
 ( #12684, #96433, #57893, #36026 ),
 .UNSPECIFIED., .F., .F.,
 ( 4, 4 ),
 ( 0.000000000000000000, 1.000000000000000000 ),
 .UNSPECIFIED. ) ;
#22988=CARTESIAN_POINT ( 'NONE',  ( -63.58953762381671027, -23.48783264082478084, -1.443836473390069042 ) ) ;
#22989=CARTESIAN_POINT ( 'NONE',  ( -1.563627757057377110, -21.15500258984412696, 11.49999999999998934 ) ) ;
#22991=CARTESIAN_POINT ( 'NONE',  ( -95.62287095715005592, -23.47593901973091235, -1.443836447539001089 ) ) ;
#22992=CARTESIAN_POINT ( 'NONE',  ( -80.47485683444980964, -25.03138299481809881, 7.562833672617995440 ) ) ;
#22994=CARTESIAN_POINT ( 'NONE',  ( -52.52287095715009713, -23.48783264083416356, -1.443836473375487151 ) ) ;
#22995=CARTESIAN_POINT ( 'NONE',  ( -16.24122463664219396, 10.56255597858309869, -1.500000000000002220 ) ) ;
#22997=FACE_BOUND ( 'NONE', #17103, .T. ) ;
#22998=ORIENTED_EDGE ( 'NONE', *, *, #84369, .F. ) ;
#22999=CARTESIAN_POINT ( 'NONE',  ( -17.65537929698502495, 8.214918384300796461, 11.49999999999999645 ) ) ;
#23000=PLANE ( 'NONE',  #16298 ) ;
#23004=CARTESIAN_POINT ( 'NONE',  ( -70.43033145357846081, -25.30470252700990130, 4.855686547977941636 ) ) ;
#23005=CARTESIAN_POINT ( 'NONE',  ( -31.52287095715006160, -29.50248528299804818, 1.056150453629029817 ) ) ;
#23007=CARTESIAN_POINT ( 'NONE',  ( -34.55620429048339304, -23.48786465467240347, 11.44779295918255713 ) ) ;
#23008=CARTESIAN_POINT ( 'NONE',  ( 5.117700956428186565, 18.95590836763280862, 11.49999999999998934 ) ) ;
#23009=CARTESIAN_POINT ( 'NONE',  ( -40.99816688406356491, -25.27806108203015967, 4.936760908640943413 ) ) ;
#23011=ORIENTED_EDGE ( 'NONE', *, *, #12539, .T. ) ;
#23012=CARTESIAN_POINT ( 'NONE',  ( 5.819084965910729323, 20.79142713412266730, -1.500000000000002220 ) ) ;
#23014=CARTESIAN_POINT ( 'NONE',  ( -40.57482487591116893, -24.92564183028978775, 1.928384488918254203 ) ) ;
#23016=CARTESIAN_POINT ( 'NONE',  ( -19.45891602060003578, 12.32625358835968576, -1.500000000000002220 ) ) ;
#23018=CARTESIAN_POINT ( 'NONE',  ( -126.6228709571500559, -23.47593901973091235, -1.443836447538995760 ) ) ;
#23020=CARTESIAN_POINT ( 'NONE',  ( -121.5532436822344664, -24.66019654487200441, 8.947790411086119278 ) ) ;
#23021=CARTESIAN_POINT ( 'NONE',  ( -101.8589946837564639, -25.21195325642122498, 6.589545632284776744 ) ) ;
#23022=B_SPLINE_CURVE_WITH_KNOTS ( 'NONE', 3,
 ( #66929, #45583, #7007, #37954, #30338, #53698 ),
 .UNSPECIFIED., .F., .F.,
 ( 4, 2, 4 ),
 ( 0.000000000000000000, 0.001380764517853252287, 0.002761529035706504574 ),
 .UNSPECIFIED. ) ;
#23023=CARTESIAN_POINT ( 'NONE',  ( -111.2413225215033634, -25.10921443801264985, 3.153769387664755008 ) ) ;
#23024=CARTESIAN_POINT ( 'NONE',  ( -129.5558834519471247, -24.15543982623907482, -0.2315651400026527140 ) ) ;
#23025=CARTESIAN_POINT ( 'NONE',  ( -99.12822588951706848, -25.26400712817571304, 4.142262319587673325 ) ) ;
#23026=CARTESIAN_POINT ( 'NONE',  ( 12.81631318294326505, -15.22695477405695996, -1.500000000000002220 ) ) ;
#23027=CARTESIAN_POINT ( 'NONE',  ( -32.62287095715004881, -29.50250786944525672, 11.44777988621624409 ) ) ;
#23028=CARTESIAN_POINT ( 'NONE',  ( 10.49454761162020588, -16.79419365751139637, -1.500000000000002220 ) ) ;
#23031=CARTESIAN_POINT ( 'NONE',  ( -37.52287095715006870, -24.65952944569304250, 1.056160979905691910 ) ) ;
#23032=CARTESIAN_POINT ( 'NONE',  ( -17.53982812869053731, -11.02811673548155902, 11.49999999999999645 ) ) ;
#23035=CARTESIAN_POINT ( 'NONE',  ( -49.76870215116556295, -25.25138707665752236, 5.358736815735848147 ) ) ;
#23036=CARTESIAN_POINT ( 'NONE',  ( 5.860688371469950475, 21.97560254587667217, 11.49999999999999645 ) ) ;
#23038=ORIENTED_EDGE ( 'NONE', *, *, #68951, .F. ) ;
#23042=CARTESIAN_POINT ( 'NONE',  ( -52.58953762381671027, -23.47596703998600276, 11.44779298504227505 ) ) ;
#23044=CARTESIAN_POINT ( 'NONE',  ( 20.19498477198788322, 0.2509159868347127231, 11.49999999999998934 ) ) ;
#23045=CARTESIAN_POINT ( 'NONE',  ( -93.52287095715006160, -29.50250786944525672, 11.44777988621623344 ) ) ;
#23046=ADVANCED_FACE ( 'NONE', ( #98201 ), #95253, .T. ) ;
#23047=DIRECTION ( 'NONE',  ( 0.000000000000000000, 0.9999999999976377785, 2.173523156925979975E-06 ) ) ;
#23048=EDGE_CURVE ( 'NONE', #33967, #17763, #36822, .T. ) ;
#23049=ORIENTED_EDGE ( 'NONE', *, *, #48370, .F. ) ;
#23050=EDGE_CURVE ( 'NONE', #2140, #6243, #98708, .T. ) ;
#23051=ORIENTED_EDGE ( 'NONE', *, *, #98841, .T. ) ;
#23053=CARTESIAN_POINT ( 'NONE',  ( 2.875404258304424143, 22.71175023210845012, -1.500000000000002220 ) ) ;
#23054=CARTESIAN_POINT ( 'NONE',  ( -51.15490599271181082, -25.27420631276300966, 3.607700143673106208 ) ) ;
#23055=CARTESIAN_POINT ( 'NONE',  ( 9.069627533930374241, 19.64968329815391712, -1.500000000000002220 ) ) ;
#23056=CARTESIAN_POINT ( 'NONE',  ( -100.6228709571500559, -29.50250243563736774, 8.947779886222138046 ) ) ;
#23057=CARTESIAN_POINT ( 'NONE',  ( -114.6228709571500559, -23.72747288104470087, -1.053458166803225460 ) ) ;
#23059=CARTESIAN_POINT ( 'NONE',  ( -11.35812032211249090, 17.58211214940072864, 11.49999999999999645 ) ) ;
#23060=ORIENTED_EDGE ( 'NONE', *, *, #15558, .T. ) ;
#23062=CARTESIAN_POINT ( 'NONE',  ( -69.08877929746488178, -25.24754397370021053, 5.548814464877763974 ) ) ;
#23063=CARTESIAN_POINT ( 'NONE',  ( -19.13726171168348245, 10.91495894028074432, -1.500000000000002220 ) ) ;
#23064=CARTESIAN_POINT ( 'NONE',  ( -105.5156638583312798, -24.15602025860896163, 10.28564288303535967 ) ) ;
#23065=CARTESIAN_POINT ( 'NONE',  ( -30.47287095715006799, -24.76053341945900499, 1.389474774145630587 ) ) ;
#23068=DIRECTION ( 'NONE',  ( -3.773278334444166432E-23, 1.000000000000000000, 0.000000000000000000 ) ) ;
#23069=EDGE_LOOP ( 'NONE', ( #42231, #15020, #52072, #39307 ) ) ;
#23070=CARTESIAN_POINT ( 'NONE',  ( -72.53829674254417625, -24.66019654487199730, 8.947790411086121054 ) ) ;
#23071=ORIENTED_EDGE ( 'NONE', *, *, #58186, .T. ) ;
#23072=ORIENTED_EDGE ( 'NONE', *, *, #67009, .F. ) ;
#23073=CARTESIAN_POINT ( 'NONE',  ( -71.49517126166168168, -24.66019654487199730, 8.947790411086113949 ) ) ;
#23074=CARTESIAN_POINT ( 'NONE',  ( -83.52287095715007581, -24.50321055353804667, 9.387540953477524042 ) ) ;
#23076=CARTESIAN_POINT ( 'NONE',  ( -18.82070947631147106, 8.064391923812276985, -1.500000000000002220 ) ) ;
#23079=CARTESIAN_POINT ( 'NONE',  ( -116.5562042904833788, -24.66019654487200086, 8.947790411086121054 ) ) ;
#23082=CARTESIAN_POINT ( 'NONE',  ( 13.76814385225720372, 17.53657229028232223, 11.49999999999998934 ) ) ;
#23083=B_SPLINE_CURVE_WITH_KNOTS ( 'NONE', 3,
 ( #20513, #75300, #97645, #99133, #60108, #90532 ),
 .UNSPECIFIED., .F., .F.,
 ( 4, 2, 4 ),
 ( 6.391158118952235087E-06, 0.001387004593080770317, 0.002767618028042588118 ),
 .UNSPECIFIED. ) ;
#23088=ORIENTED_EDGE ( 'NONE', *, *, #71737, .T. ) ;
#23089=CARTESIAN_POINT ( 'NONE',  ( -27.70544111104076990, -24.60484793945295934, 1.628749883096155981 ) ) ;
#23090=CARTESIAN_POINT ( 'NONE',  ( -29.70813536620188700, -25.26247646271292524, 6.270927263681702613 ) ) ;
#23092=CARTESIAN_POINT ( 'NONE',  ( -12.40256906124370673, -16.71776976679197801, -1.500000000000002220 ) ) ;
#23093=EDGE_LOOP ( 'NONE', ( #25835, #21738, #58089, #24515 ) ) ;
#23099=ORIENTED_EDGE ( 'NONE', *, *, #89542, .T. ) ;
#23100=PLANE ( 'NONE',  #49532 ) ;
#23105=CARTESIAN_POINT ( 'NONE',  ( -109.8721775411165424, -25.13089038914449347, 2.890306159589083101 ) ) ;
#23106=CARTESIAN_POINT ( 'NONE',  ( -53.52287095715008292, -23.48783264082477018, -1.443836473390094799 ) ) ;
#23107=CARTESIAN_POINT ( 'NONE',  ( 20.56832688555235222, -8.368550285707721414, 11.49999999999999645 ) ) ;
#23108=ORIENTED_EDGE ( 'NONE', *, *, #62024, .T. ) ;
#23109=CARTESIAN_POINT ( 'NONE',  ( -44.62287095715005592, -23.73934037231755667, 11.05740245334329508 ) ) ;
#23111=CARTESIAN_POINT ( 'NONE',  ( 20.84710439121840864, 8.857176948214046774, -1.500000000000002220 ) ) ;
#23113=CARTESIAN_POINT ( 'NONE',  ( -115.5956212965460850, -23.48786465467241769, 11.44779295918253581 ) ) ;
#23114=ORIENTED_EDGE ( 'NONE', *, *, #35263, .T. ) ;
#23115=ORIENTED_EDGE ( 'NONE', *, *, #40866, .F. ) ;
#23116=CARTESIAN_POINT ( 'NONE',  ( -112.6228709571500559, -23.47596703998600631, 11.44779298504227860 ) ) ;
#23117=EDGE_CURVE ( 'NONE', #65831, #61715, #38559, .T. ) ;
#23119=CARTESIAN_POINT ( 'NONE',  ( -18.49208213979201076, -7.923680710433813168, -1.500000000000002220 ) ) ;
#23120=LINE ( 'NONE', #92143, #24650 ) ;
#23122=CARTESIAN_POINT ( 'NONE',  ( -37.62287095715005592, -29.50250243563736774, 8.947779886222148704 ) ) ;
#23123=CARTESIAN_POINT ( 'NONE',  ( 22.31825301297700648, 1.237144038376295274, -1.500000000000002220 ) ) ;
#23124=VERTEX_POINT ( 'NONE', #33195 ) ;
#23127=VECTOR ( 'NONE', #3788, 1000.000000000000114 ) ;
#23128=CARTESIAN_POINT ( 'NONE',  ( -94.54500761342549708, -24.66019654487199730, 8.947790411086121054 ) ) ;
#23130=CARTESIAN_POINT ( 'NONE',  ( -59.52287095715006160, -24.64898659630528854, 1.056161002820822592 ) ) ;
#23132=CARTESIAN_POINT ( 'NONE',  ( 4.865394487973861537, 18.91859722749940786, -1.500000000000002220 ) ) ;
#23135=CARTESIAN_POINT ( 'NONE',  ( 21.49998558720804809, 0.1351929536555107336, -1.500000000000002220 ) ) ;
#23136=CARTESIAN_POINT ( 'NONE',  ( -62.52287095715006160, -23.48786465467241058, 11.44779295918254824 ) ) ;
#23137=FACE_OUTER_BOUND ( 'NONE', #97868, .T. ) ;
#23140=CARTESIAN_POINT ( 'NONE',  ( 22.22072617242880455, -5.352622178732230118, -1.500000000000002220 ) ) ;
#23144=CARTESIAN_POINT ( 'NONE',  ( -4.751880754313710042, -19.48972053015312866, 11.49999999999999645 ) ) ;
#23146=CARTESIAN_POINT ( 'NONE',  ( -118.6228709571500559, -23.47593901973091235, -1.443836447538997536 ) ) ;
#23147=CARTESIAN_POINT ( 'NONE',  ( 6.026614999332422182E-17, -23.47594215783195537, -5.102550391006585557E-05 ) ) ;
#23152=CARTESIAN_POINT ( 'NONE',  ( -1.994712787082457472, 21.64621699974126656, 11.49999999999998934 ) ) ;
#23154=CARTESIAN_POINT ( 'NONE',  ( -19.37001648656083574, -3.113731218521536004, -1.500000000000002220 ) ) ;
#23156=VECTOR ( 'NONE', #49648, 1000.000000000000114 ) ;
#23157=CARTESIAN_POINT ( 'NONE',  ( -109.5669895805274336, -25.31698083318981318, 4.843009121909479298 ) ) ;
#23160=CARTESIAN_POINT ( 'NONE',  ( -91.50904508725861319, -24.35071581493543391, 9.817618358456025263 ) ) ;
#23162=CARTESIAN_POINT ( 'NONE',  ( 7.506095096478735407, 19.11734572241606145, 11.49999999999999645 ) ) ;
#23164=FACE_OUTER_BOUND ( 'NONE', #37612, .T. ) ;
#23166=ADVANCED_FACE ( 'NONE', ( #46424 ), #34269, .T. ) ;
#23167=ORIENTED_EDGE ( 'NONE', *, *, #19687, .F. ) ;
#23168=CARTESIAN_POINT ( 'NONE',  ( -83.55620429048339304, -23.47596703998600276, 11.44779298504227683 ) ) ;
#23169=CARTESIAN_POINT ( 'NONE',  ( -69.62287095715005592, -24.65952944569304961, 1.056160979905697017 ) ) ;
#23170=CARTESIAN_POINT ( 'NONE',  ( -125.5540156586789067, -25.00182538069147498, 7.747789668545045139 ) ) ;
#23172=CARTESIAN_POINT ( 'NONE',  ( -67.62287095715005592, -29.50248528299804818, 1.056150453629036701 ) ) ;
#23174=B_SPLINE_CURVE_WITH_KNOTS ( 'NONE', 3,
 ( #64625, #41260, #93523, #95540, #15902, #62597, #16400, #78298, #39743, #94032, #24518, #55486, #81812, #35646, #58001, #88933 ),
 .UNSPECIFIED., .F., .F.,
 ( 4, 2, 2, 2, 2, 2, 2, 4 ),
 ( 0.000000000000000000, 0.0002240477605849928056, 0.0004480955211699856112, 0.0008961910423400092779, 0.001120238802925007694, 0.001344286563510006544, 0.001568334324095004961, 0.001792382084680003811 ),
 .UNSPECIFIED. ) ;
#23175=CARTESIAN_POINT ( 'NONE',  ( -25.81215951358583993, -24.93063326169846761, 6.831251959621990721 ) ) ;
#23177=PLANE ( 'NONE',  #25316 ) ;
#23178=B_SPLINE_CURVE_WITH_KNOTS ( 'NONE', 3,
 ( #11391, #95129, #34239, #34734 ),
 .UNSPECIFIED., .F., .F.,
 ( 4, 4 ),
 ( 0.000000000000000000, 1.000000000000000000 ),
 .UNSPECIFIED. ) ;
#23180=B_SPLINE_CURVE_WITH_KNOTS ( 'NONE', 3,
 ( #42017, #88182, #4447, #18651 ),
 .UNSPECIFIED., .F., .F.,
 ( 4, 4 ),
 ( 0.000000000000000000, 1.000000000000000000 ),
 .UNSPECIFIED. ) ;
#23181=CARTESIAN_POINT ( 'NONE',  ( -22.28253579152010033, 6.022996098971622914, 11.49999999999999645 ) ) ;
#23182=CARTESIAN_POINT ( 'NONE',  ( 17.57702471007113232, 14.52005670271990034, -1.500000000000002220 ) ) ;
#23183=CARTESIAN_POINT ( 'NONE',  ( -33.92287095715005307, -23.47596703998600276, 11.44779298504227683 ) ) ;
#23184=B_SPLINE_SURFACE_WITH_KNOTS ( 'NONE', 3, 3, ( 
 ( #15188, #100401, #30914, #68485 ),
 ( #30415, #91811, #31419, #15690 ),
 ( #99420, #93304, #46656, #62376 ),
 ( #61884, #22284, #23288, #23797 ),
 ( #77575, #92311, #16186, #47156 ),
 ( #7580, #31924, #70487, #46151 ),
 ( #78073, #8585, #29914, #8080 ),
 ( #52762, #53267, #77075, #38528 ),
 ( #93815, #92806, #69486, #39027 ),
 ( #39534, #83699, #84195, #6580 ) ),
 .UNSPECIFIED., .F., .F., .F.,
 ( 4, 3, 3, 4 ),
 ( 4, 4 ),
 ( 0.0004766839783815726879, 0.1491231665100170301, 0.2234464077758347433, 0.2977696490416524844 ),
 ( 0.4995543325860023476, 0.5008647392976423030 ),
 .UNSPECIFIED. ) ;
#23187=CARTESIAN_POINT ( 'NONE',  ( -64.22287095715006444, -23.47593901973090169, -1.443836447538997536 ) ) ;
#23188=CARTESIAN_POINT ( 'NONE',  ( -20.53624283083718893, 9.024085183690161216, 11.49999999999999645 ) ) ;
#23189=EDGE_LOOP ( 'NONE', ( #84856, #64551, #52840, #74430 ) ) ;
#23193=CARTESIAN_POINT ( 'NONE',  ( 20.11839708684271244, 8.774209887332036217, -1.500000000000002220 ) ) ;
#23194=CARTESIAN_POINT ( 'NONE',  ( -113.5228709571500616, -24.65952944569304961, 1.056160979905704123 ) ) ;
#23195=CARTESIAN_POINT ( 'NONE',  ( -45.52287095715006160, -23.48786465467240347, 11.44779295918255002 ) ) ;
#23196=CARTESIAN_POINT ( 'NONE',  ( -104.6235422183511758, -24.65952944569305316, 1.056160979905702346 ) ) ;
#23197=CARTESIAN_POINT ( 'NONE',  ( -78.56384845838088893, -23.48783264082477018, -1.443836473390096797 ) ) ;
#23199=ORIENTED_EDGE ( 'NONE', *, *, #45425, .F. ) ;
#23200=CARTESIAN_POINT ( 'NONE',  ( -18.53176153473302179, -8.692061069824589481, -1.500000000000002220 ) ) ;
#23201=ORIENTED_EDGE ( 'NONE', *, *, #69853, .T. ) ;
#23202=VERTEX_POINT ( 'NONE', #93581 ) ;
#23203=ORIENTED_EDGE ( 'NONE', *, *, #75831, .T. ) ;
#23204=ORIENTED_EDGE ( 'NONE', *, *, #97162, .F. ) ;
#23205=CARTESIAN_POINT ( 'NONE',  ( -17.14199295335891904, -15.44578658782692671, -1.500000000000002220 ) ) ;
#23206=CARTESIAN_POINT ( 'NONE',  ( -40.79613026685809274, -25.30524842186639844, 5.093185296294494790 ) ) ;
#23207=CARTESIAN_POINT ( 'NONE',  ( 0.7445296356392017145, -20.29553345556499622, -1.500000000000002220 ) ) ;
#23210=CARTESIAN_POINT ( 'NONE',  ( -29.26526703061216494, -25.20409411716389769, 4.938174481708933250 ) ) ;
#23211=CARTESIAN_POINT ( 'NONE',  ( -92.59143168555947057, -24.15543982623908192, -0.2315651400026453588 ) ) ;
#23212=CARTESIAN_POINT ( 'NONE',  ( -101.3562811213368775, -25.19976993852609937, 6.677978858547927388 ) ) ;
#23213=CARTESIAN_POINT ( 'NONE',  ( -65.62287095715005592, -29.50247984919015209, -1.443849546365055359 ) ) ;
#23214=CARTESIAN_POINT ( 'NONE',  ( -11.62584540149672385, -18.10649092712023389, 11.49999999999999645 ) ) ;
#23215=ORIENTED_EDGE ( 'NONE', *, *, #80707, .F. ) ;
#23216=CARTESIAN_POINT ( 'NONE',  ( -75.62935843874419106, -24.73486907724918282, 1.287355809206967683 ) ) ;
#23217=CARTESIAN_POINT ( 'NONE',  ( -34.62287095715004881, -24.50216790748203266, 0.6166512839542577229 ) ) ;
#23218=AXIS2_PLACEMENT_3D ( 'NONE', #80469, #51526, #95697 ) ;
#23220=CARTESIAN_POINT ( 'NONE',  ( -7.464567774302189207, 19.34240081622845153, -1.500000000000002220 ) ) ;
#23221=ORIENTED_EDGE ( 'NONE', *, *, #39535, .F. ) ;
#23223=EDGE_LOOP ( 'NONE', ( #39946, #75889, #44133, #43667 ) ) ;
#23228=CARTESIAN_POINT ( 'NONE',  ( -116.6228709571500275, -23.47596703998600631, 11.44779298504227860 ) ) ;
#23229=CARTESIAN_POINT ( 'NONE',  ( -76.52287095715007581, -23.48786465467241769, 11.44779295918254469 ) ) ;
#23230=CARTESIAN_POINT ( 'NONE',  ( 15.37660858059359725, 15.65766701038582021, 11.49999999999999645 ) ) ;
#23232=CARTESIAN_POINT ( 'NONE',  ( 18.83488669200175281, -12.41447709603701632, 11.49999999999998934 ) ) ;
#23233=CARTESIAN_POINT ( 'NONE',  ( -8.674659061502078217, -19.08593140856894621, 11.49999999999998934 ) ) ;
#23234=CARTESIAN_POINT ( 'NONE',  ( -48.52287095715004739, -23.48783264083430211, -1.443836473375264440 ) ) ;
#23235=VECTOR ( 'NONE', #46659, 1000.000000000000114 ) ;
#23236=PLANE ( 'NONE',  #94556 ) ;
#23239=ORIENTED_EDGE ( 'NONE', *, *, #19652, .F. ) ;
#23240=CARTESIAN_POINT ( 'NONE',  ( -72.52287095715007581, -24.64898659630367916, 1.056161002820824368 ) ) ;
#23242=CARTESIAN_POINT ( 'NONE',  ( -18.53595284743415661, 10.95218985133829825, -1.500000000000002220 ) ) ;
#23243=VECTOR ( 'NONE', #58025, 1000.000000000000114 ) ;
#23245=DIRECTION ( 'NONE',  ( -3.773278334453080206E-23, 0.9999999999976377785, 2.173523156925979975E-06 ) ) ;
#23247=CARTESIAN_POINT ( 'NONE',  ( 3.428800225705347149, -20.88102749682517612, -1.500000000000002220 ) ) ;
#23248=CARTESIAN_POINT ( 'NONE',  ( -83.58953762381673869, -24.64898659630528854, 1.056161002820828587 ) ) ;
#23249=CARTESIAN_POINT ( 'NONE',  ( -58.85933311957388980, -25.20144863547804803, 6.835696751361012957 ) ) ;
#23250=CARTESIAN_POINT ( 'NONE',  ( -49.51097411295445028, -25.26741039762233498, 4.038287390307901958 ) ) ;
#23251=DIRECTION ( 'NONE',  ( 3.773278334444167608E-23, -1.000000000000000000, 0.000000000000000000 ) ) ;
#23253=CARTESIAN_POINT ( 'NONE',  ( 17.03105324785762420, 14.15717209551829647, -1.500000000000002220 ) ) ;
#23259=CARTESIAN_POINT ( 'NONE',  ( -5.843762028675351772, -18.45606589188993141, 11.49999999999999645 ) ) ;
#23261=CARTESIAN_POINT ( 'NONE',  ( 19.29218144733592055, -2.436590042558338443, 11.49999999999998934 ) ) ;
#23262=CARTESIAN_POINT ( 'NONE',  ( -15.71168838272081558, 14.50144224353281786, 11.49999999999998934 ) ) ;
#23265=CARTESIAN_POINT ( 'NONE',  ( -40.58953762381672448, -25.00158670708908559, 2.256160236439166411 ) ) ;
#23266=CARTESIAN_POINT ( 'NONE',  ( -100.4839344043725333, -25.18440011564083747, 3.295732011862015032 ) ) ;
#23267=CARTESIAN_POINT ( 'NONE',  ( -22.58250372949163420, -2.080990182559540269, -1.500000000000002220 ) ) ;
#23268=B_SPLINE_SURFACE_WITH_KNOTS ( 'NONE', 3, 3, ( 
 ( #84749, #5256, #77626, #82379 ),
 ( #36214, #70028, #43826, #28103 ),
 ( #35719, #69538, #15237, #515 ),
 ( #91861, #22829, #53817, #20 ),
 ( #67178, #14731, #77125, #15738 ),
 ( #74761, #22333, #7632, #38580 ),
 ( #59061, #62429, #92858, #85755 ) ),
 .UNSPECIFIED., .F., .F., .F.,
 ( 4, 3, 4 ),
 ( 4, 4 ),
 ( 0.0004766839783819774206, 0.1029713700210896365, 0.2054660560637973088 ),
 ( 0.3895931030775385828, 0.3907855851754823417 ),
 .UNSPECIFIED. ) ;
#23269=CARTESIAN_POINT ( 'NONE',  ( -106.5228709571500900, -23.47593901973090524, -1.443836447538996204 ) ) ;
#23270=CARTESIAN_POINT ( 'NONE',  ( -57.62287095715004170, -23.73934037231756733, 11.05740245334329153 ) ) ;
#23271=CARTESIAN_POINT ( 'NONE',  ( -6.239078800006583769, 18.87631364486404806, 11.49999999999999645 ) ) ;
#23274=CARTESIAN_POINT ( 'NONE',  ( -73.62287095715004170, -23.72747288104441665, -1.053458166803662888 ) ) ;
#23275=ORIENTED_EDGE ( 'NONE', *, *, #10265, .T. ) ;
#23276=PLANE ( 'NONE',  #59119 ) ;
#23277=DIRECTION ( 'NONE',  ( -4.522247983293619802E-39, -2.173523156893721996E-06, 0.9999999999976377785 ) ) ;
#23278=DIRECTION ( 'NONE',  ( -3.773278334453079618E-23, 0.9999999999976377785, 2.173523156925979975E-06 ) ) ;
#23279=CARTESIAN_POINT ( 'NONE',  ( 21.02075834227166951, -5.193550065563941942, 11.49999999999998934 ) ) ;
#23281=CARTESIAN_POINT ( 'NONE',  ( 16.20606029192996900, -10.75321813762353251, -1.500000000000002220 ) ) ;
#23283=CARTESIAN_POINT ( 'NONE',  ( -55.53127495292982729, -24.83644354573578283, 8.397322867130096569 ) ) ;
#23284=CARTESIAN_POINT ( 'NONE',  ( 18.55763160240848109, 7.024834138330111166, 11.49999999999998934 ) ) ;
#23287=CARTESIAN_POINT ( 'NONE',  ( -9.641467040090685003, 17.89903724589931855, 11.49999999999999645 ) ) ;
#23288=CARTESIAN_POINT ( 'NONE',  ( -80.54797791650044303, -24.40034930558991277, 0.3402023900116063482 ) ) ;
#23289=CARTESIAN_POINT ( 'NONE',  ( -41.52287095715006870, -23.47593901973090169, -1.443836447538997092 ) ) ;
#23290=EDGE_LOOP ( 'NONE', ( #97481, #21957, #81540, #36937 ) ) ;
#23291=CARTESIAN_POINT ( 'NONE',  ( -41.05394856697249395, -25.21735233672366405, 3.457401395030163638 ) ) ;
#23293=CARTESIAN_POINT ( 'NONE',  ( -49.43920486724100982, -25.25214466810134795, 5.121422890020069119 ) ) ;
#23295=CARTESIAN_POINT ( 'NONE',  ( -40.61243824264953872, -23.85049219812685095, 10.88485053497527488 ) ) ;
#23297=CARTESIAN_POINT ( 'NONE',  ( 16.71511084712224360, -11.16500066668146829, 11.49999999999998934 ) ) ;
#23298=B_SPLINE_CURVE_WITH_KNOTS ( 'NONE', 3,
 ( #17660, #93273, #31889, #47625, #32893, #23763 ),
 .UNSPECIFIED., .F., .F.,
 ( 4, 2, 4 ),
 ( 0.000000000000000000, 0.001380901958385383991, 0.002761803916770767982 ),
 .UNSPECIFIED. ) ;
#23299=FACE_OUTER_BOUND ( 'NONE', #23223, .T. ) ;
#23301=VERTEX_POINT ( 'NONE', #9353 ) ;
#23304=CARTESIAN_POINT ( 'NONE',  ( -17.51315278866654879, 14.73147661606379621, 11.49999999999999645 ) ) ;
#23305=CARTESIAN_POINT ( 'NONE',  ( -13.58842472641693711, -18.21064416987719525, 11.49999999999998934 ) ) ;
#23306=VERTEX_POINT ( 'NONE', #94593 ) ;
#23307=CARTESIAN_POINT ( 'NONE',  ( -45.52287095715006870, -24.52232992886360918, 0.6492154411905974865 ) ) ;
#23309=CARTESIAN_POINT ( 'NONE',  ( -126.5228709571499763, -23.73934037231757443, 11.05740245334327909 ) ) ;
#23310=CARTESIAN_POINT ( 'NONE',  ( -38.56093905060389915, -23.73791477778911485, 11.05961554403170766 ) ) ;
#23311=EDGE_CURVE ( 'NONE', #78575, #29423, #36237, .T. ) ;
#23312=CARTESIAN_POINT ( 'NONE',  ( -30.57287095715006231, -23.48210175247266562, -1.443836490256470428 ) ) ;
#23313=CARTESIAN_POINT ( 'NONE',  ( -128.6234765682969510, -24.66019654487200441, 8.947790411086108620 ) ) ;
#23316=CARTESIAN_POINT ( 'NONE',  ( 8.549789220347504326, 18.50885834720105905, -1.500000000000002220 ) ) ;
#23317=EDGE_LOOP ( 'NONE', ( #22558, #88667, #20463, #21602 ) ) ;
#23318=EDGE_CURVE ( 'NONE', #89515, #55826, #66453, .T. ) ;
#23319=CARTESIAN_POINT ( 'NONE',  ( 20.04565040668967413, 11.27863464804978477, 11.49999999999998934 ) ) ;
#23320=CARTESIAN_POINT ( 'NONE',  ( -54.64430529514193324, -23.96169478059712787, 10.65365249895718947 ) ) ;
#23321=ORIENTED_EDGE ( 'NONE', *, *, #86480, .T. ) ;
#23322=CARTESIAN_POINT ( 'NONE',  ( -34.62287095715005592, -29.50248528299804818, 1.056150453629029817 ) ) ;
#23323=CARTESIAN_POINT ( 'NONE',  ( -81.39414160900706463, -25.21421764495619300, 6.570651892964196605 ) ) ;
#23325=CARTESIAN_POINT ( 'NONE',  ( 9.569808575145499319, 19.01914523534739132, 11.49999999999999645 ) ) ;
#23327=VERTEX_POINT ( 'NONE', #49441 ) ;
#23328=CARTESIAN_POINT ( 'NONE',  ( 2.577866586777615154, 22.04066829813923789, -1.500000000000002220 ) ) ;
#23329=CARTESIAN_POINT ( 'NONE',  ( -13.08992234710881064, 15.94516925376868244, 11.49999999999998934 ) ) ;
#23330=B_SPLINE_CURVE_WITH_KNOTS ( 'NONE', 3,
 ( #78162, #32006, #71584, #62979 ),
 .UNSPECIFIED., .F., .F.,
 ( 4, 4 ),
 ( 0.000000000000000000, 9.999999999998897304E-05 ),
 .UNSPECIFIED. ) ;
#23334=CARTESIAN_POINT ( 'NONE',  ( -95.62359480617779184, -25.00182538069147142, 7.747789668545044250 ) ) ;
#23336=CARTESIAN_POINT ( 'NONE',  ( -51.62287095715006302, -23.96177878511307924, 10.65340807706330217 ) ) ;
#23338=CARTESIAN_POINT ( 'NONE',  ( -56.62287095715005592, -24.64965695001468404, 8.947790433994185832 ) ) ;
#23339=DIRECTION ( 'NONE',  ( 1.000000000000000000, 3.773278334444166432E-23, 8.201307841325785021E-29 ) ) ;
#23340=CARTESIAN_POINT ( 'NONE',  ( -20.21371806590929410, -4.994250807877889109, -1.500000000000002220 ) ) ;
#23341=CARTESIAN_POINT ( 'NONE',  ( 17.22188757068894915, 13.35947340969901198, 11.49999999999999645 ) ) ;
#23342=VECTOR ( 'NONE', #51168, 1000.000000000000227 ) ;
#23344=CARTESIAN_POINT ( 'NONE',  ( -78.54012698005728055, -24.66019654487200441, 8.947790411086119278 ) ) ;
#23345=CARTESIAN_POINT ( 'NONE',  ( -22.33494257564923302, 2.542849975942539587, -1.500000000000002220 ) ) ;
#23346=CARTESIAN_POINT ( 'NONE',  ( -50.47686723370601669, -25.31296764644767094, 4.734242616601387788 ) ) ;
#23348=ORIENTED_EDGE ( 'NONE', *, *, #78908, .T. ) ;
#23352=VERTEX_POINT ( 'NONE', #43320 ) ;
#23353=VERTEX_POINT ( 'NONE', #79864 ) ;
#23354=EDGE_CURVE ( 'NONE', #62407, #9013, #26534, .T. ) ;
#23356=CARTESIAN_POINT ( 'NONE',  ( 19.59546714036918758, 8.467717511154198462, -1.500000000000002220 ) ) ;
#23357=EDGE_LOOP ( 'NONE', ( #62315, #78102, #614, #61698 ) ) ;
#23358=CARTESIAN_POINT ( 'NONE',  ( 18.99863377428308198, 9.053671573812124507, -1.500000000000002220 ) ) ;
#23359=CARTESIAN_POINT ( 'NONE',  ( -30.44999254588300985, -24.04395793212950849, -0.4713115009884517037 ) ) ;
#23360=CARTESIAN_POINT ( 'NONE',  ( -110.9769629572514447, -25.22239614775561023, 3.498991103823542836 ) ) ;
#23362=CARTESIAN_POINT ( 'NONE',  ( 19.92286461850947887, -9.344431347164146473, -1.500000000000002220 ) ) ;
#23365=FACE_OUTER_BOUND ( 'NONE', #69719, .T. ) ;
#23366=CARTESIAN_POINT ( 'NONE',  ( -121.5228709571500474, -23.72747288104470442, -1.053458166803224794 ) ) ;
#23367=CARTESIAN_POINT ( 'NONE',  ( -20.21371806590929410, -4.994250807877889109, 11.49999999999999645 ) ) ;
#23368=CARTESIAN_POINT ( 'NONE',  ( -74.58953762381673869, -24.65952944569304606, 1.056160979905703234 ) ) ;
#23369=CARTESIAN_POINT ( 'NONE',  ( -108.6228709571500417, -23.48786465467242479, 11.44779295918253759 ) ) ;
#23370=B_SPLINE_CURVE_WITH_KNOTS ( 'NONE', 3,
 ( #85291, #69070, #45244, #99503 ),
 .UNSPECIFIED., .F., .F.,
 ( 4, 4 ),
 ( 0.000000000000000000, 0.0001000000000000167422 ),
 .UNSPECIFIED. ) ;
#23371=CARTESIAN_POINT ( 'NONE',  ( -10.22955294603096732, -23.25643961109228641, 8.370978854367626454 ) ) ;
#23372=CARTESIAN_POINT ( 'NONE',  ( 14.87313431965483801, 15.23822737908125902, -1.500000000000002220 ) ) ;
#23373=CARTESIAN_POINT ( 'NONE',  ( -98.63501790545433323, -23.73791477778911840, 11.05961554403170410 ) ) ;
#23374=CARTESIAN_POINT ( 'NONE',  ( -107.6317652604150936, -23.73791477778912196, 11.05961554403169700 ) ) ;
#23376=CARTESIAN_POINT ( 'NONE',  ( -71.31920756328558753, -25.12112739299269037, 7.112216829152949948 ) ) ;
#23378=CARTESIAN_POINT ( 'NONE',  ( -22.13300264024875119, -4.194623038110560032, -1.500000000000002220 ) ) ;
#23379=CARTESIAN_POINT ( 'NONE',  ( -65.52287095715006160, -25.00158670708909625, 2.256160236439166411 ) ) ;
#23381=CARTESIAN_POINT ( 'NONE',  ( -123.5228709571500616, -24.64898659630368627, 1.056161002820833028 ) ) ;
#23382=CARTESIAN_POINT ( 'NONE',  ( 16.12930680145378304, -11.13525102954884893, 11.49999999999999645 ) ) ;
#23384=CARTESIAN_POINT ( 'NONE',  ( -32.52287095715004739, -23.96177878511307213, 10.65340807706330750 ) ) ;
#23388=CARTESIAN_POINT ( 'NONE',  ( -90.93395226104127005, -25.22174524493127379, 6.695141717414600180 ) ) ;
#23389=CARTESIAN_POINT ( 'NONE',  ( 19.26447527235507451, 4.322997736827044690, -1.500000000000002220 ) ) ;
#23390=EDGE_LOOP ( 'NONE', ( #21428, #66236, #51099, #9334 ) ) ;
#23393=B_SPLINE_CURVE_WITH_KNOTS ( 'NONE', 3,
 ( #52208, #98363, #35976, #11634 ),
 .UNSPECIFIED., .F., .F.,
 ( 4, 4 ),
 ( 1.387778780781445521E-17, 0.0001000000000000028644 ),
 .UNSPECIFIED. ) ;
#23395=ORIENTED_EDGE ( 'NONE', *, *, #79345, .F. ) ;
#23396=PLANE ( 'NONE',  #51596 ) ;
#23398=CARTESIAN_POINT ( 'NONE',  ( -55.48264273398157798, -24.83618233451448987, 1.606449574219538379 ) ) ;
#23401=CARTESIAN_POINT ( 'NONE',  ( -44.62287095715004881, -24.64965695001468404, 8.947790433994187609 ) ) ;
#23402=CARTESIAN_POINT ( 'NONE',  ( -107.5502841407374035, -24.51314013834316086, 0.6176544820404228364 ) ) ;
#23403=CARTESIAN_POINT ( 'NONE',  ( -19.89792590360708147, -2.209704250470923892, 11.49999999999998934 ) ) ;
#23404=ADVANCED_FACE ( 'NONE', ( #73269 ), #70928, .T. ) ;
#23407=CARTESIAN_POINT ( 'NONE',  ( -45.52502077163275374, -24.92592662359561118, 8.075495903018000021 ) ) ;
#23408=ORIENTED_EDGE ( 'NONE', *, *, #55125, .T. ) ;
#23409=DIRECTION ( 'NONE',  ( -3.773278334453079030E-23, 0.9999999999976377785, 2.173523156925979128E-06 ) ) ;
#23410=DIRECTION ( 'NONE',  ( -3.773278334453079618E-23, 0.9999999999976377785, 2.173523156925979975E-06 ) ) ;
#23411=EDGE_CURVE ( 'NONE', #33324, #12246, #83355, .T. ) ;
#23415=CARTESIAN_POINT ( 'NONE',  ( -116.4728709571500360, -25.40558663563427189, 5.000950442582703381 ) ) ;
#23416=B_SPLINE_CURVE_WITH_KNOTS ( 'NONE', 3,
 ( #10021, #87655, #2930, #70428 ),
 .UNSPECIFIED., .F., .F.,
 ( 4, 4 ),
 ( 3.244156161651605912E-05, 0.008792202774406619389 ),
 .UNSPECIFIED. ) ;
#23417=CARTESIAN_POINT ( 'NONE',  ( -83.58828318951894687, -24.34968618360933235, 0.1864209137778810865 ) ) ;
#23419=PLANE ( 'NONE',  #58267 ) ;
#23420=ORIENTED_EDGE ( 'NONE', *, *, #3715, .F. ) ;
#23421=CARTESIAN_POINT ( 'NONE',  ( 16.58868386459195676, 11.68684615565071283, 11.49999999999998934 ) ) ;
#23422=EDGE_CURVE ( 'NONE', #6116, #9400, #62857, .T. ) ;
#23423=DIRECTION ( 'NONE',  ( -2.145277261456712182E-39, -2.173523156925979128E-06, 0.9999999999976378895 ) ) ;
#23424=DIRECTION ( 'NONE',  ( -3.773278334444167608E-23, 1.000000000000000000, 0.000000000000000000 ) ) ;
#23426=CARTESIAN_POINT ( 'NONE',  ( -86.52287095715009002, -24.51387760970724727, 9.387446482453409402 ) ) ;
#23427=CARTESIAN_POINT ( 'NONE',  ( -7.807601069497579260, -18.53474111305376937, -1.500000000000002220 ) ) ;
#23428=CARTESIAN_POINT ( 'NONE',  ( 14.35337761433406811, 15.45585641580067104, 11.49999999999999645 ) ) ;
#23430=CARTESIAN_POINT ( 'NONE',  ( 1.014068502963303864, -22.09113584270698993, 11.49999999999998934 ) ) ;
#23431=CARTESIAN_POINT ( 'NONE',  ( -9.284664653622879626, 18.31210316397345395, 11.49999999999998934 ) ) ;
#23432=CARTESIAN_POINT ( 'NONE',  ( -65.62287095715005592, -25.00182538069145721, 7.747789668545100206 ) ) ;
#23433=CARTESIAN_POINT ( 'NONE',  ( -60.65501980248554048, -23.85016227208579664, -0.8807180028928355275 ) ) ;
#23434=ORIENTED_EDGE ( 'NONE', *, *, #33159, .F. ) ;
#23437=DIRECTION ( 'NONE',  ( 0.000000000000000000, 0.9999999999976377785, 2.173523156925979975E-06 ) ) ;
#23438=B_SPLINE_SURFACE_WITH_KNOTS ( 'NONE', 3, 3, ( 
 ( #93865, #2039, #2535, #70535 ),
 ( #17242, #31469, #62431, #16739 ),
 ( #77629, #32981, #54822, #25356 ),
 ( #70032, #56334, #85758, #63956 ),
 ( #63446, #1532, #15741, #33467 ),
 ( #86259, #93357, #87254, #46706 ),
 ( #518, #71545, #40088, #41097 ) ),
 .UNSPECIFIED., .F., .F., .F.,
 ( 4, 3, 4 ),
 ( 4, 4 ),
 ( 0.7945040050992243641, 0.8970133687736503436, 0.9995227324480763231 ),
 ( 0.7196768771113082330, 0.7210218522699133326 ),
 .UNSPECIFIED. ) ;
#23439=B_SPLINE_CURVE_WITH_KNOTS ( 'NONE', 3,
 ( #39098, #55348, #16762, #48233, #79164, #40113 ),
 .UNSPECIFIED., .F., .F.,
 ( 4, 2, 4 ),
 ( 1.570755371633816901E-05, 0.001396183895866085368, 0.002776660238015832543 ),
 .UNSPECIFIED. ) ;
#23440=CARTESIAN_POINT ( 'NONE',  ( -85.62287095714999907, -24.15516710230295772, 10.28746687063726739 ) ) ;
#23442=ORIENTED_EDGE ( 'NONE', *, *, #17341, .F. ) ;
#23443=VERTEX_POINT ( 'NONE', #99561 ) ;
#23445=CARTESIAN_POINT ( 'NONE',  ( -31.58953762381672092, -23.47593901973091235, -1.443836447539013301 ) ) ;
#23446=PLANE ( 'NONE',  #40658 ) ;
#23447=CARTESIAN_POINT ( 'NONE',  ( -1.706377481887368486, -20.59057665607738130, -1.500000000000002220 ) ) ;
#23449=CARTESIAN_POINT ( 'NONE',  ( -19.46174652491427182, -9.421329337880418819, 11.49999999999999645 ) ) ;
#23450=ORIENTED_EDGE ( 'NONE', *, *, #79079, .F. ) ;
#23453=CARTESIAN_POINT ( 'NONE',  ( -8.633843874998758494, 20.65557450359631630, 11.49999999999998934 ) ) ;
#23454=CARTESIAN_POINT ( 'NONE',  ( -47.51395832360446292, -23.73791477778911485, 11.05961554403170766 ) ) ;
#23457=B_SPLINE_CURVE_WITH_KNOTS ( 'NONE', 3,
 ( #97872, #37487, #13136, #67447, #52221, #28370 ),
 .UNSPECIFIED., .F., .F.,
 ( 4, 2, 4 ),
 ( 1.570887131794333942E-05, 0.001396322306279760422, 0.002776935741241577573 ),
 .UNSPECIFIED. ) ;
#23458=CARTESIAN_POINT ( 'NONE',  ( -116.4728709572980847, -25.40561136713226276, 5.197834629370922777 ) ) ;
#23461=CARTESIAN_POINT ( 'NONE',  ( -19.94816486946033507, 6.322790147265108018, -1.500000000000002220 ) ) ;
#23464=CARTESIAN_POINT ( 'NONE',  ( -67.56551492114158464, -23.48786465467241058, 11.44779295918254824 ) ) ;
#23465=EDGE_LOOP ( 'NONE', ( #62808, #32197, #63542, #6058 ) ) ;
#23466=EDGE_CURVE ( 'NONE', #83268, #3631, #70007, .T. ) ;
#23467=FACE_OUTER_BOUND ( 'NONE', #38011, .T. ) ;
#23468=CARTESIAN_POINT ( 'NONE',  ( -21.15187133135857422, -0.9709546189074961253, -1.500000000000002220 ) ) ;
#23470=CARTESIAN_POINT ( 'NONE',  ( -50.50118616174772512, -24.15503026093912808, -0.2815557561904566963 ) ) ;
#23471=CARTESIAN_POINT ( 'NONE',  ( -14.02725853290852243, 16.66567569088042688, 11.49999999999998934 ) ) ;
#23472=DIRECTION ( 'NONE',  ( 0.000000000000000000, -0.9999999999976377785, -2.173523156925979128E-06 ) ) ;
#23473=CARTESIAN_POINT ( 'NONE',  ( -84.52287095715006160, -23.47593901973090524, -1.443836447538996648 ) ) ;
#23474=CARTESIAN_POINT ( 'NONE',  ( -35.52287095715008292, -24.14406661686761524, 10.28769366194079282 ) ) ;
#23475=CARTESIAN_POINT ( 'NONE',  ( -8.041798833237560729, -20.28069125152608976, -1.500000000000002220 ) ) ;
#23476=CARTESIAN_POINT ( 'NONE',  ( -95.52287095715011844, -24.92579138211019796, 1.929029949965664459 ) ) ;
#23477=EDGE_LOOP ( 'NONE', ( #89234, #93385, #41527, #10108 ) ) ;
#23484=B_SPLINE_CURVE_WITH_KNOTS ( 'NONE', 3,
 ( #75919, #82051, #68325, #90164 ),
 .UNSPECIFIED., .F., .F.,
 ( 4, 4 ),
 ( 0.000000000000000000, 0.0001000000000000028644 ),
 .UNSPECIFIED. ) ;
#23485=ORIENTED_EDGE ( 'NONE', *, *, #18656, .F. ) ;
#23487=CARTESIAN_POINT ( 'NONE',  ( -39.62287095715005592, -23.47593901973091235, -1.443836447539011525 ) ) ;
#23488=CARTESIAN_POINT ( 'NONE',  ( -19.34623641613454836, -8.721557147202650739, 11.49999999999998934 ) ) ;
#23489=CARTESIAN_POINT ( 'NONE',  ( -121.6228709571500701, -24.33832256526968862, 0.1851278514119947260 ) ) ;
#23490=CARTESIAN_POINT ( 'NONE',  ( -79.32136430576915131, -25.27791861366366533, 7.049788063976406782 ) ) ;
#23491=CARTESIAN_POINT ( 'NONE',  ( -104.6228709571500559, -23.48783264082478794, -1.443836473390062158 ) ) ;
#23492=CARTESIAN_POINT ( 'NONE',  ( -99.52287095715009002, -23.47593901973090524, -1.443836447538996648 ) ) ;
#23493=ADVANCED_FACE ( 'NONE', ( #69132 ), #99071, .T. ) ;
#23495=CARTESIAN_POINT ( 'NONE',  ( 14.41255161864883583, -12.98630880007775268, -1.500000000000002220 ) ) ;
#23496=CARTESIAN_POINT ( 'NONE',  ( -39.02522392549908403, -25.31392318313163159, 5.203682277190879724 ) ) ;
#23498=CARTESIAN_POINT ( 'NONE',  ( 8.422564666779264186, -17.53554878399664574, 11.49999999999999645 ) ) ;
#23500=EDGE_CURVE ( 'NONE', #95766, #19712, #92997, .T. ) ;
#23502=ORIENTED_EDGE ( 'NONE', *, *, #48148, .T. ) ;
#23504=EDGE_CURVE ( 'NONE', #93563, #59914, #31379, .T. ) ;
#23505=CARTESIAN_POINT ( 'NONE',  ( -65.52287095715006160, -29.50250243563736774, 8.947779886222143375 ) ) ;
#23506=ADVANCED_FACE ( 'NONE', ( #52925 ), #59541, .F. ) ;
#23509=CARTESIAN_POINT ( 'NONE',  ( 5.239555828037883778, -18.94419173073049478, -1.500000000000002220 ) ) ;
#23510=CARTESIAN_POINT ( 'NONE',  ( -41.39099037118809576, -25.27806020386471531, 4.532732343367795735 ) ) ;
#23512=EDGE_CURVE ( 'NONE', #7527, #25743, #98072, .T. ) ;
#23514=CARTESIAN_POINT ( 'NONE',  ( 10.40854797073303395, 18.91789161722374146, 11.49999999999998934 ) ) ;
#23515=CARTESIAN_POINT ( 'NONE',  ( -40.64049736129675949, -24.52300882791530157, 0.6510814631126359275 ) ) ;
#23516=CARTESIAN_POINT ( 'NONE',  ( -121.5228709571500616, -24.64898659630529565, 1.056161002820833028 ) ) ;
#23517=CARTESIAN_POINT ( 'NONE',  ( -17.35246277222573141, 15.15038115719275424, -1.500000000000002220 ) ) ;
#23518=B_SPLINE_CURVE_WITH_KNOTS ( 'NONE', 3,
 ( #86994, #23079, #16473, #56065 ),
 .UNSPECIFIED., .F., .F.,
 ( 4, 4 ),
 ( 2.775557561562891043E-17, 9.999999999998898659E-05 ),
 .UNSPECIFIED. ) ;
#23519=MECHANICAL_CONTEXT ( 'NONE', #42716, 'mechanical' ) ;
#23520=CARTESIAN_POINT ( 'NONE',  ( -126.5228709571500616, -29.50250243563736774, 8.947779886222132717 ) ) ;
#23521=CARTESIAN_POINT ( 'NONE',  ( -115.6228709571500559, -23.47593901973091235, -1.443836447538997536 ) ) ;
#23522=CARTESIAN_POINT ( 'NONE',  ( -121.5186303220462776, -24.51419770103157347, 9.386484678747175181 ) ) ;
#23524=CARTESIAN_POINT ( 'NONE',  ( -111.7148472136480990, -25.29824037455150076, 3.873545699286501165 ) ) ;
#23525=FACE_OUTER_BOUND ( 'NONE', #4159, .T. ) ;
#23526=B_SPLINE_CURVE_WITH_KNOTS ( 'NONE', 3,
 ( #4684, #88922, #26010, #20380 ),
 .UNSPECIFIED., .F., .F.,
 ( 4, 4 ),
 ( 0.9794846856643069088, 0.9804854327050720464 ),
 .UNSPECIFIED. ) ;
#23527=CARTESIAN_POINT ( 'NONE',  ( -114.6254316867186844, -24.35071581493544102, 9.817618358456016381 ) ) ;
#23528=CARTESIAN_POINT ( 'NONE',  ( -9.044204435542846809, 17.70297415775587169, 11.49999999999998934 ) ) ;
#23531=CARTESIAN_POINT ( 'NONE',  ( 10.41257876278241845, -16.90412932818451353, -1.500000000000002220 ) ) ;
#23534=CARTESIAN_POINT ( 'NONE',  ( -39.04303308397305727, -25.29116819090583235, 4.215216924258844422 ) ) ;
#23536=CARTESIAN_POINT ( 'NONE',  ( 4.358738815032396907, -20.29635662749097236, 11.49999999999999645 ) ) ;
#23537=CARTESIAN_POINT ( 'NONE',  ( -94.52287095715007581, -23.47593901973090524, -1.443836447538996648 ) ) ;
#23539=EDGE_CURVE ( 'NONE', #80523, #88227, #94273, .T. ) ;
#23540=CARTESIAN_POINT ( 'NONE',  ( -106.5551948350586429, -23.96119346886880663, -0.6495511937832030291 ) ) ;
#23541=CARTESIAN_POINT ( 'NONE',  ( -20.37646751746074969, -10.17465561509698979, 11.49999999999999645 ) ) ;
#23544=CARTESIAN_POINT ( 'NONE',  ( -69.55927295150912926, -23.73766607897669445, -1.055555164236460008 ) ) ;
#23546=CARTESIAN_POINT ( 'NONE',  ( -92.52287095715010423, -24.33927499327853994, 9.819080762295806508 ) ) ;
#23549=CARTESIAN_POINT ( 'NONE',  ( -19.56588111578679090, -4.897929960003377658, 11.49999999999998934 ) ) ;
#23550=PLANE ( 'NONE',  #48417 ) ;
#23551=EDGE_CURVE ( 'NONE', #56734, #3816, #99110, .T. ) ;
#23553=CARTESIAN_POINT ( 'NONE',  ( -52.52287095715005449, -23.95044443724991723, 10.65354141964649592 ) ) ;
#23555=AXIS2_PLACEMENT_3D ( 'NONE', #20335, #59934, #14224 ) ;
#23557=B_SPLINE_CURVE_WITH_KNOTS ( 'NONE', 3,
 ( #45270, #20912, #68110, #89939 ),
 .UNSPECIFIED., .F., .F.,
 ( 4, 4 ),
 ( 0.000000000000000000, 9.999999999998900014E-05 ),
 .UNSPECIFIED. ) ;
#23559=CARTESIAN_POINT ( 'NONE',  ( -101.6228709571500701, -23.47596703998600631, 11.44779298504227683 ) ) ;
#23560=CARTESIAN_POINT ( 'NONE',  ( 1.119804705421552748, 22.86502198858056545, -1.500000000000002220 ) ) ;
#23561=CARTESIAN_POINT ( 'NONE',  ( -50.49777224651334961, -25.18439650350726922, 3.296419330453493224 ) ) ;
#23563=CARTESIAN_POINT ( 'NONE',  ( 21.13687465659472409, 4.681744431724916389, -1.500000000000002220 ) ) ;
#23564=CARTESIAN_POINT ( 'NONE',  ( -123.6234902428110303, -24.65952944569305316, 1.056160979905707897 ) ) ;
#23565=CARTESIAN_POINT ( 'NONE',  ( 8.587038044527741221, -19.06309208085484386, 11.49999999999999645 ) ) ;
#23566=ORIENTED_EDGE ( 'NONE', *, *, #22270, .T. ) ;
#23567=CARTESIAN_POINT ( 'NONE',  ( -124.5895435931244322, -24.34968618360933945, 0.1864209137778899961 ) ) ;
#23568=CARTESIAN_POINT ( 'NONE',  ( -12.30081598482267680, 18.28176383447183895, -1.500000000000002220 ) ) ;
#23570=CARTESIAN_POINT ( 'NONE',  ( -65.62287095715004170, -24.91570333823099759, 8.075032458375558164 ) ) ;
#23571=ORIENTED_EDGE ( 'NONE', *, *, #3070, .T. ) ;
#23572=DIRECTION ( 'NONE',  ( 0.000000000000000000, -0.9999999999976377785, -2.173523156925979975E-06 ) ) ;
#23575=DIRECTION ( 'NONE',  ( 3.773278334444167608E-23, -1.000000000000000000, 0.000000000000000000 ) ) ;
#23576=ORIENTED_EDGE ( 'NONE', *, *, #50288, .F. ) ;
#23578=CARTESIAN_POINT ( 'NONE',  ( -71.60771150786226258, -23.48786465467241058, 11.44779295918254824 ) ) ;
#23579=CARTESIAN_POINT ( 'NONE',  ( -101.3783285514244028, -25.27404712219727401, 3.208885956357566460 ) ) ;
#23580=CARTESIAN_POINT ( 'NONE',  ( -100.5228709571500758, -24.62285846331434058, 9.038163153548365969 ) ) ;
#23581=CARTESIAN_POINT ( 'NONE',  ( -3.437008290023895185, 20.19323497536227663, -1.500000000000002220 ) ) ;
#23582=ORIENTED_EDGE ( 'NONE', *, *, #73377, .T. ) ;
#23583=CARTESIAN_POINT ( 'NONE',  ( -79.52287095715006160, -24.64898659630367916, 1.056161002820826145 ) ) ;
#23584=CARTESIAN_POINT ( 'NONE',  ( -44.63404635305053603, -24.34968618360933235, 0.1864209137778787551 ) ) ;
#23585=LINE ( 'NONE', #69281, #72620 ) ;
#23586=CARTESIAN_POINT ( 'NONE',  ( -14.60993195340527251, 16.82711592829100411, -1.500000000000002220 ) ) ;
#23587=CARTESIAN_POINT ( 'NONE',  ( -71.29814285433251086, -25.24267958441406634, 6.333824918460533304 ) ) ;
#23590=DIRECTION ( 'NONE',  ( -3.773278334453079618E-23, 0.9999999999976377785, 2.173523156925979975E-06 ) ) ;
#23593=CARTESIAN_POINT ( 'NONE',  ( 5.313885144808909722, 20.14914662543312929, -1.500000000000002220 ) ) ;
#23594=ORIENTED_EDGE ( 'NONE', *, *, #76958, .T. ) ;
#23595=CARTESIAN_POINT ( 'NONE',  ( -95.52287095715010423, -25.00182538069145366, 7.747789668545101982 ) ) ;
#23596=ORIENTED_EDGE ( 'NONE', *, *, #47945, .T. ) ;
#23599=CARTESIAN_POINT ( 'NONE',  ( -8.441512789788195192, 19.21024974253229800, -1.500000000000002220 ) ) ;
#23602=CARTESIAN_POINT ( 'NONE',  ( -50.44065031394416820, -25.27412228105976055, 2.834208053142886818 ) ) ;
#23603=B_SPLINE_CURVE_WITH_KNOTS ( 'NONE', 3,
 ( #12039, #43007, #43990, #5923 ),
 .UNSPECIFIED., .F., .F.,
 ( 4, 4 ),
 ( 0.000000000000000000, 1.000000000000000000 ),
 .UNSPECIFIED. ) ;
#23606=CARTESIAN_POINT ( 'NONE',  ( -92.54439753425451443, -24.66019654487200441, 8.947790411086117501 ) ) ;
#23607=CARTESIAN_POINT ( 'NONE',  ( -65.62287095715005592, -23.85229601348996198, 10.88205029486208986 ) ) ;
#23608=CARTESIAN_POINT ( 'NONE',  ( -4.330935931041660858, -21.79039167146679290, 11.49999999999999645 ) ) ;
#23609=VERTEX_POINT ( 'NONE', #23432 ) ;
#23611=CARTESIAN_POINT ( 'NONE',  ( -61.62287095715004881, -29.50248528299804818, 1.056150453629034924 ) ) ;
#23613=CARTESIAN_POINT ( 'NONE',  ( 9.629844747126790949, -20.51516216672183290, 11.49999999999998934 ) ) ;
#23614=CARTESIAN_POINT ( 'NONE',  ( -28.94417065657630062, -25.04901277059179776, 6.781005994535155068 ) ) ;
#23615=EDGE_LOOP ( 'NONE', ( #8271, #10917, #80162, #65330, #17290, #80662 ) ) ;
#23616=ORIENTED_EDGE ( 'NONE', *, *, #92847, .F. ) ;
#23617=CARTESIAN_POINT ( 'NONE',  ( -67.92287095715008149, -23.47596703998600276, 11.44779298504227683 ) ) ;
#23618=VECTOR ( 'NONE', #54172, 1000.000000000000114 ) ;
#23620=CARTESIAN_POINT ( 'NONE',  ( 19.31759285448427477, -5.727529672960866236, 11.49999999999998934 ) ) ;
#23621=CARTESIAN_POINT ( 'NONE',  ( -81.62287095715004170, -23.48786465467241058, 11.44779295918254647 ) ) ;
#23622=VERTEX_POINT ( 'NONE', #41081 ) ;
#23623=VECTOR ( 'NONE', #93254, 1000.000000000000114 ) ;
#23625=CARTESIAN_POINT ( 'NONE',  ( -15.27869365379592281, -16.34152646814254339, -1.500000000000002220 ) ) ;
#23626=VECTOR ( 'NONE', #90797, 1000.000000000000114 ) ;
#23631=CARTESIAN_POINT ( 'NONE',  ( -94.54704744228577340, -24.51419770103156281, 9.386484678747184063 ) ) ;
#23632=CARTESIAN_POINT ( 'NONE',  ( -85.55620429048339304, -23.47596703998600631, 11.44779298504227683 ) ) ;
#23633=EDGE_CURVE ( 'NONE', #73650, #71376, #59242, .T. ) ;
#23636=VECTOR ( 'NONE', #41426, 1000.000000000000114 ) ;
#23637=EDGE_CURVE ( 'NONE', #7900, #78003, #71274, .T. ) ;
#23639=CARTESIAN_POINT ( 'NONE',  ( 19.54226456527178257, 0.3027743077981833730, -1.500000000000002220 ) ) ;
#23640=CARTESIAN_POINT ( 'NONE',  ( -39.22287095715006444, -23.47596703998600276, 11.44779298504227683 ) ) ;
#23641=EDGE_CURVE ( 'NONE', #67908, #71832, #92458, .T. ) ;
#23642=CARTESIAN_POINT ( 'NONE',  ( 11.78165356204951131, -17.99452314462042324, -1.500000000000002220 ) ) ;
#23643=B_SPLINE_CURVE_WITH_KNOTS ( 'NONE', 3,
 ( #54408, #1632, #9733, #63543, #87351, #55417 ),
 .UNSPECIFIED., .F., .F.,
 ( 4, 2, 4 ),
 ( 1.570755371634013412E-05, 0.001396183895866088187, 0.002776660238015836012 ),
 .UNSPECIFIED. ) ;
#23645=CARTESIAN_POINT ( 'NONE',  ( -114.5228709571500616, -24.64898659630529565, 1.056161002820831474 ) ) ;
#23646=CARTESIAN_POINT ( 'NONE',  ( -91.52287095715006160, -24.64965694238575011, 8.947790433994196491 ) ) ;
#23648=CARTESIAN_POINT ( 'NONE',  ( -22.23020047961643186, 5.420056861400933457, -1.500000000000002220 ) ) ;
#23651=CARTESIAN_POINT ( 'NONE',  ( -71.29940687171418290, -25.26721001298331970, 6.088028500398946719 ) ) ;
#23652=CARTESIAN_POINT ( 'NONE',  ( -11.57650325489309395, -16.32560983125179277, 11.49999999999999645 ) ) ;
#23653=CARTESIAN_POINT ( 'NONE',  ( -80.06557898417501917, -25.31594321096806510, 4.529242715578940093 ) ) ;
#23655=DIRECTION ( 'NONE',  ( 2.567145104890970367E-18, -0.9999999999976378895, -2.173523156893722419E-06 ) ) ;
#23657=ORIENTED_EDGE ( 'NONE', *, *, #58171, .T. ) ;
#23658=CARTESIAN_POINT ( 'NONE',  ( -50.62287095715005592, -25.00182538069145011, 7.747789668545097541 ) ) ;
#23659=EDGE_CURVE ( 'NONE', #44696, #6687, #13206, .T. ) ;
#23661=CARTESIAN_POINT ( 'NONE',  ( -16.08361747308824263, -14.67194924222005170, -1.500000000000002220 ) ) ;
#23662=CARTESIAN_POINT ( 'NONE',  ( -45.52287095715007581, -25.00182538069144655, 7.747789668545101094 ) ) ;
#23663=CARTESIAN_POINT ( 'NONE',  ( -19.15055961920884542, -4.482958728538418924, -1.500000000000002220 ) ) ;
#23664=CARTESIAN_POINT ( 'NONE',  ( -128.5228709571500758, -24.64898659630368627, 1.056161002820834804 ) ) ;
#23665=EDGE_CURVE ( 'NONE', #21356, #28727, #7732, .T. ) ;
#23666=CARTESIAN_POINT ( 'NONE',  ( -109.3640311185025098, -25.27925697487621548, 4.352105652871627761 ) ) ;
#23668=CARTESIAN_POINT ( 'NONE',  ( -66.62287095715005592, -29.50250243563736774, 8.947779886222143375 ) ) ;
#23669=DIRECTION ( 'NONE',  ( -3.773278334453079618E-23, 0.9999999999976377785, 2.173523156925979975E-06 ) ) ;
#23670=CARTESIAN_POINT ( 'NONE',  ( 7.647619880454145758, 19.11525441646967849, 11.49999999999999645 ) ) ;
#23671=CARTESIAN_POINT ( 'NONE',  ( -39.04717630401307105, -25.29744946566268382, 4.335755123932833577 ) ) ;
#23672=EDGE_CURVE ( 'NONE', #41110, #53182, #18234, .T. ) ;
#23673=CARTESIAN_POINT ( 'NONE',  ( -120.6228709571500417, -24.99132157543166954, 2.256160258750667502 ) ) ;
#23674=ORIENTED_EDGE ( 'NONE', *, *, #47785, .F. ) ;
#23675=CARTESIAN_POINT ( 'NONE',  ( -100.6814946224345846, -25.26387453836298747, 4.736250637429614940 ) ) ;
#23676=CARTESIAN_POINT ( 'NONE',  ( -27.53137588795584634, -24.79921317967766825, 7.599174398616137971 ) ) ;
#23677=CARTESIAN_POINT ( 'NONE',  ( -125.5543383043813463, -24.83644354573579349, 8.397322867130096569 ) ) ;
#23681=CARTESIAN_POINT ( 'NONE',  ( -43.62287095715004881, -29.50250786944525672, 11.44777988621624232 ) ) ;
#23683=ADVANCED_FACE ( 'NONE', ( #69643 ), #94412, .T. ) ;
#23684=VERTEX_POINT ( 'NONE', #75004 ) ;
#23685=CARTESIAN_POINT ( 'NONE',  ( 22.88022663504679599, 2.825535151426334934, 11.49999999999999645 ) ) ;
#23686=CARTESIAN_POINT ( 'NONE',  ( 17.58993269669914383, -14.52173041563253975, -1.500000000000002220 ) ) ;
#23688=CARTESIAN_POINT ( 'NONE',  ( -96.52217812738990688, -23.48783264082477018, -1.443836473390089914 ) ) ;
#23689=CARTESIAN_POINT ( 'NONE',  ( -57.52287095715004739, -23.94994826722564696, -0.6494450866342742490 ) ) ;
#23690=CARTESIAN_POINT ( 'NONE',  ( 22.22467975111640470, 2.813832150844377100, 11.49999999999999645 ) ) ;
#23692=LINE ( 'NONE', #92702, #86527 ) ;
#23693=FACE_OUTER_BOUND ( 'NONE', #85112, .T. ) ;
#23694=EDGE_CURVE ( 'NONE', #85301, #7254, #74024, .T. ) ;
#23695=CARTESIAN_POINT ( 'NONE',  ( 1.885617179787854036, 21.85875792104173598, 11.49999999999998934 ) ) ;
#23699=LINE ( 'NONE', #95225, #3309 ) ;
#23701=CARTESIAN_POINT ( 'NONE',  ( -125.6228709571500559, -24.99156045073393173, 7.747789690856161648 ) ) ;
#23705=CARTESIAN_POINT ( 'NONE',  ( 12.80116962295325322, 15.99954467330607244, -1.500000000000002220 ) ) ;
#23708=VERTEX_POINT ( 'NONE', #21217 ) ;
#23709=ORIENTED_EDGE ( 'NONE', *, *, #74744, .T. ) ;
#23711=CARTESIAN_POINT ( 'NONE',  ( 0.1381291366035634904, -23.06709338131901532, 11.49999999999998934 ) ) ;
#23712=CARTESIAN_POINT ( 'NONE',  ( -39.43380829106687457, -25.30524842186639844, 5.093185296294494790 ) ) ;
#23713=CARTESIAN_POINT ( 'NONE',  ( 2.303441031721801480, -20.17751241584783628, -1.500000000000002220 ) ) ;
#23717=LINE ( 'NONE', #31336, #77354 ) ;
#23719=CARTESIAN_POINT ( 'NONE',  ( -89.81226385320384509, -25.32787472568953646, 4.644766527794375044 ) ) ;
#23721=CARTESIAN_POINT ( 'NONE',  ( -0.9917595143200197416, 21.46465604038169772, 11.49999999999999645 ) ) ;
#23722=ORIENTED_EDGE ( 'NONE', *, *, #84884, .F. ) ;
#23723=CARTESIAN_POINT ( 'NONE',  ( -75.49989344710095907, -24.52300882791530157, 0.6510814631126414787 ) ) ;
#23724=CARTESIAN_POINT ( 'NONE',  ( -61.63194629385022694, -24.35071581493543036, 9.817618358456030592 ) ) ;
#23726=CARTESIAN_POINT ( 'NONE',  ( 12.91705851660734972, -16.24616318834520001, 11.49999999999998934 ) ) ;
#23728=B_SPLINE_CURVE_WITH_KNOTS ( 'NONE', 3,
 ( #31995, #55349, #40620, #16268, #86281, #62965 ),
 .UNSPECIFIED., .F., .F.,
 ( 4, 2, 4 ),
 ( 6.391158118952234240E-06, 0.001387004593080773352, 0.002767618028042594189 ),
 .UNSPECIFIED. ) ;
#23731=CARTESIAN_POINT ( 'NONE',  ( -75.62287095715004170, -24.82576562982390911, 8.398263435472971494 ) ) ;
#23732=CARTESIAN_POINT ( 'NONE',  ( -53.52287095715007581, -24.51283580621364777, 0.6167428607019670439 ) ) ;
#23736=CARTESIAN_POINT ( 'NONE',  ( -77.62287095715007013, -24.33927499327854704, 9.819080762295822495 ) ) ;
#23737=B_SPLINE_CURVE_WITH_KNOTS ( 'NONE', 3,
 ( #90934, #92923, #92427, #15804 ),
 .UNSPECIFIED., .F., .F.,
 ( 4, 4 ),
 ( 1.387778780781445676E-17, 0.0004038461538461435296 ),
 .UNSPECIFIED. ) ;
#23738=CARTESIAN_POINT ( 'NONE',  ( -65.58378039220416156, -24.73486907724918282, 1.287355809206962354 ) ) ;
#23739=CARTESIAN_POINT ( 'NONE',  ( -6.199593828526920092, 21.14725108817225419, 11.49999999999999645 ) ) ;
#23741=CARTESIAN_POINT ( 'NONE',  ( 15.74396088501716839, 16.14010210793005839, -1.500000000000002220 ) ) ;
#23743=CARTESIAN_POINT ( 'NONE',  ( 11.23609023086081038, -17.74952302366565604, 11.49999999999998934 ) ) ;
#23744=CARTESIAN_POINT ( 'NONE',  ( -105.5895376238167387, -23.47593901973091235, -1.443836447538999312 ) ) ;
#23745=EDGE_LOOP ( 'NONE', ( #62988, #12508, #85750, #48629 ) ) ;
#23747=CARTESIAN_POINT ( 'NONE',  ( -53.52287095715008292, -23.48783264082477018, -1.443836473390094799 ) ) ;
#23750=CARTESIAN_POINT ( 'NONE',  ( -1.424071398598787397, -21.11453822904667277, -1.500000000000002220 ) ) ;
#23751=DIRECTION ( 'NONE',  ( -1.000000000000000000, -3.773278334444167608E-23, -8.201307833595939069E-29 ) ) ;
#23753=CARTESIAN_POINT ( 'NONE',  ( -59.79414125094724852, -25.20144863547804803, 6.835696751361012957 ) ) ;
#23755=LINE ( 'NONE', #69444, #83226 ) ;
#23756=CARTESIAN_POINT ( 'NONE',  ( -47.62287095715005592, -23.95044443724990657, 10.65354141964650125 ) ) ;
#23757=CARTESIAN_POINT ( 'NONE',  ( 21.55033589006239936, 5.121329677682045833, -1.500000000000002220 ) ) ;
#23758=EDGE_CURVE ( 'NONE', #27620, #28558, #21451, .T. ) ;
#23759=CARTESIAN_POINT ( 'NONE',  ( -71.55402992468556533, -23.96119346886880308, -0.6495511937832095795 ) ) ;
#23760=EDGE_CURVE ( 'NONE', #57700, #78091, #83115, .T. ) ;
#23761=EDGE_LOOP ( 'NONE', ( #20910, #39936, #20462, #90927 ) ) ;
#23762=CARTESIAN_POINT ( 'NONE',  ( -51.72290159494567519, -25.24860110716892692, 5.484618035424846383 ) ) ;
#23763=CARTESIAN_POINT ( 'NONE',  ( -64.62287095715005592, -24.64965695001468404, 8.947790433994185832 ) ) ;
#23764=CARTESIAN_POINT ( 'NONE',  ( -126.5558604981289790, -23.96119346886880663, -0.6495511937832031402 ) ) ;
#23765=ADVANCED_FACE ( 'NONE', ( #19226 ), #28847, .F. ) ;
#23768=B_SPLINE_CURVE_WITH_KNOTS ( 'NONE', 3,
 ( #83176, #60376, #45634, #44632 ),
 .UNSPECIFIED., .F., .F.,
 ( 4, 4 ),
 ( 0.000000000000000000, 0.0001000000000000167422 ),
 .UNSPECIFIED. ) ;
#23769=CARTESIAN_POINT ( 'NONE',  ( -84.62287095715007013, -23.48786465467241769, 11.44779295918254469 ) ) ;
#23770=CARTESIAN_POINT ( 'NONE',  ( 18.80106323769845389, 4.952424739525837616, -1.500000000000002220 ) ) ;
#23771=CARTESIAN_POINT ( 'NONE',  ( 17.72605931280000391, -11.99821887194124770, 11.49999999999998934 ) ) ;
#23772=CARTESIAN_POINT ( 'NONE',  ( -38.52287095715007581, -24.51387760970724372, 9.387446482453404073 ) ) ;
#23773=CARTESIAN_POINT ( 'NONE',  ( -110.2093792378192063, -25.30161501422653814, 5.585409209247975681 ) ) ;
#23775=CARTESIAN_POINT ( 'NONE',  ( -101.0947412695425385, -25.27360029102344896, 3.544729148234888161 ) ) ;
#23776=CARTESIAN_POINT ( 'NONE',  ( -18.33335541821337245, -13.34141728429830742, -1.500000000000002220 ) ) ;
#23777=AXIS2_PLACEMENT_3D ( 'NONE', #98404, #97907, #96428 ) ;
#23780=CARTESIAN_POINT ( 'NONE',  ( -110.6228709571500701, -25.00182538069145011, 7.747789668545099317 ) ) ;
#23782=CARTESIAN_POINT ( 'NONE',  ( -18.60049703728633474, -6.982253431394513932, 11.49999999999999645 ) ) ;
#23783=CARTESIAN_POINT ( 'NONE',  ( -123.6259827803453959, -23.73791477778912551, 11.05961554403169878 ) ) ;
#23785=CARTESIAN_POINT ( 'NONE',  ( -115.5228709571500616, -23.47596703998600631, 11.44779298504227860 ) ) ;
#23786=ORIENTED_EDGE ( 'NONE', *, *, #64512, .F. ) ;
#23787=FACE_OUTER_BOUND ( 'NONE', #66423, .T. ) ;
#23789=PLANE ( 'NONE',  #64270 ) ;
#23790=CARTESIAN_POINT ( 'NONE',  ( -11.49108604648090548, 18.38894055434275643, 11.49999999999998934 ) ) ;
#23792=CARTESIAN_POINT ( 'NONE',  ( -18.68671320864135765, 5.291888989699490509, -1.500000000000002220 ) ) ;
#23794=FACE_OUTER_BOUND ( 'NONE', #85393, .T. ) ;
#23796=CARTESIAN_POINT ( 'NONE',  ( 19.91419669613914678, 4.404666692190684962, 11.49999999999999645 ) ) ;
#23797=CARTESIAN_POINT ( 'NONE',  ( -80.50431331750769459, -24.40034930558991277, 0.3402023900116063482 ) ) ;
#23799=B_SPLINE_CURVE_WITH_KNOTS ( 'NONE', 3,
 ( #7556, #53745, #84675, #91779 ),
 .UNSPECIFIED., .F., .F.,
 ( 4, 4 ),
 ( 0.000000000000000000, 9.999999999998897304E-05 ),
 .UNSPECIFIED. ) ;
#23801=CARTESIAN_POINT ( 'NONE',  ( -40.76800260471102177, -25.20049804043521036, 3.332830128871373088 ) ) ;
#23803=CARTESIAN_POINT ( 'NONE',  ( -96.62287095715005592, -24.64965695001468404, 8.947790433994178727 ) ) ;
#23804=B_SPLINE_CURVE_WITH_KNOTS ( 'NONE', 3,
 ( #57738, #3947, #64366, #42016 ),
 .UNSPECIFIED., .F., .F.,
 ( 4, 4 ),
 ( 0.5008576501881971677, 0.5098640814603130345 ),
 .UNSPECIFIED. ) ;
#23805=CARTESIAN_POINT ( 'NONE',  ( -40.52054363820756322, -25.00182538069146432, 7.747789668545040698 ) ) ;
#23807=CARTESIAN_POINT ( 'NONE',  ( 1.236116150138429903, -20.07036509671028668, -1.500000000000002220 ) ) ;
#23809=VERTEX_POINT ( 'NONE', #58798 ) ;
#23811=VECTOR ( 'NONE', #45353, 1000.000000000000114 ) ;
#23812=EDGE_CURVE ( 'NONE', #3669, #642, #49358, .T. ) ;
#23813=CARTESIAN_POINT ( 'NONE',  ( 2.875404258304424143, 22.71175023210845012, 11.49999999999999645 ) ) ;
#23814=CARTESIAN_POINT ( 'NONE',  ( -22.67762270672801250, 1.536325718666671225, 11.49999999999998934 ) ) ;
#23817=PLANE ( 'NONE',  #18566 ) ;
#23818=CARTESIAN_POINT ( 'NONE',  ( -59.62287095715004881, -24.64898659630367916, 1.056161002820822592 ) ) ;
#23820=CARTESIAN_POINT ( 'NONE',  ( -98.52287095715007581, -23.47593901973090524, -1.443836447538996648 ) ) ;
#23822=CARTESIAN_POINT ( 'NONE',  ( -128.5557741445947784, -24.15620529776629510, 10.23563542870659582 ) ) ;
#23824=EDGE_LOOP ( 'NONE', ( #26050, #31071, #89159, #89259 ) ) ;
#23825=CARTESIAN_POINT ( 'NONE',  ( 12.54693703879240196, 16.07252283493236433, 11.49999999999998934 ) ) ;
#23827=CARTESIAN_POINT ( 'NONE',  ( 3.160899137004691717, 22.77513019406404382, 11.49999999999998934 ) ) ;
#23828=CARTESIAN_POINT ( 'NONE',  ( -45.52287095715006870, -24.91544648472619983, 1.928969306349231028 ) ) ;
#23829=ORIENTED_EDGE ( 'NONE', *, *, #75784, .F. ) ;
#23830=CARTESIAN_POINT ( 'NONE',  ( -62.62287095715004881, -24.66019654487199020, 8.947790411086131712 ) ) ;
#23833=CARTESIAN_POINT ( 'NONE',  ( -89.52287095715006160, -24.65952944569304606, 1.056160979905700570 ) ) ;
#23834=CARTESIAN_POINT ( 'NONE',  ( -19.99249555334884221, 7.427959064407942513, 11.49999999999999645 ) ) ;
#23836=ORIENTED_EDGE ( 'NONE', *, *, #78777, .F. ) ;
#23837=CARTESIAN_POINT ( 'NONE',  ( 19.92104321119709098, 9.795001720801039369, 11.49999999999998934 ) ) ;
#23838=B_SPLINE_CURVE_WITH_KNOTS ( 'NONE', 3,
 ( #66760, #49026, #87574, #69225 ),
 .UNSPECIFIED., .F., .F.,
 ( 4, 4 ),
 ( 0.9594697448489959424, 0.9604704918897616350 ),
 .UNSPECIFIED. ) ;
#23839=CARTESIAN_POINT ( 'NONE',  ( -1.706377481887368486, -20.59057665607738130, -1.500000000000002220 ) ) ;
#23841=VERTEX_POINT ( 'NONE', #60308 ) ;
#23843=CARTESIAN_POINT ( 'NONE',  ( -109.6203743360497214, -25.31627411512031145, 5.518883902012535536 ) ) ;
#23844=CARTESIAN_POINT ( 'NONE',  ( -95.50651195402215876, -24.63419186844610920, 9.035850630976922204 ) ) ;
#23845=EDGE_LOOP ( 'NONE', ( #18076, #32316, #72755, #10244 ) ) ;
#23846=CARTESIAN_POINT ( 'NONE',  ( -49.43404257242507782, -25.20234397918763847, 6.663189757676971858 ) ) ;
#23850=CARTESIAN_POINT ( 'NONE',  ( -112.6228709571500417, -24.66019654487199730, 8.947790411086124607 ) ) ;
#23851=CARTESIAN_POINT ( 'NONE',  ( -12.40256906124370673, -16.71776976679197801, -1.500000000000002220 ) ) ;
#23852=CARTESIAN_POINT ( 'NONE',  ( -21.66901994843296819, -2.608494568651300138, 11.49999999999999645 ) ) ;
#23853=CARTESIAN_POINT ( 'NONE',  ( -27.68651082257923335, -24.77993797811391019, 7.605672579471098871 ) ) ;
#23854=CARTESIAN_POINT ( 'NONE',  ( -78.58187020279800095, -24.66019654487200441, 8.947790411086119278 ) ) ;
#23855=CARTESIAN_POINT ( 'NONE',  ( 21.67916507323446496, -5.852930566066080864, -1.500000000000002220 ) ) ;
#23856=CARTESIAN_POINT ( 'NONE',  ( -38.56093874523811849, -23.73766607897670511, -1.055555164236442689 ) ) ;
#23857=CARTESIAN_POINT ( 'NONE',  ( -87.62287095715004170, -23.48783264082478794, -1.443836473390063269 ) ) ;
#23859=ORIENTED_EDGE ( 'NONE', *, *, #72243, .T. ) ;
#23860=ORIENTED_EDGE ( 'NONE', *, *, #42646, .T. ) ;
#23862=CARTESIAN_POINT ( 'NONE',  ( -19.64189229742525455, -8.423329616690555355, -1.500000000000002220 ) ) ;
#23864=CARTESIAN_POINT ( 'NONE',  ( -20.88184962559319402, -2.832954952542597660, -1.500000000000002220 ) ) ;
#23865=LINE ( 'NONE', #76152, #90346 ) ;
#23866=EDGE_CURVE ( 'NONE', #35546, #67048, #47014, .T. ) ;
#23867=CARTESIAN_POINT ( 'NONE',  ( -7.409219584043468920, -18.53548363135739052, -1.500000000000002220 ) ) ;
#23868=( BOUNDED_CURVE ( )  B_SPLINE_CURVE ( 3, ( #45461, #68786, #83498, #30207, #99702, #37345, #36342, #28729, #44457, #28224, #59689, #52068, #99217, #13984, #60688, #61190, #90621, #82995, #91610, #43463 ),
 .UNSPECIFIED., .F., .F. ) 
 B_SPLINE_CURVE_WITH_KNOTS ( ( 4, 3, 1, 1, 3, 3, 1, 1, 3, 4 ),
 ( 0.000000000000000000, 0.1282082775799912033, 0.1695614466321895275, 0.2109146156843880737, 0.2522677847365863979, 0.7503515196349076488, 0.7917046886871055289, 0.8330578577393035200, 0.8744110267915015111, 1.000000000000000000 ),
 .UNSPECIFIED. ) 
 CURVE ( )  GEOMETRIC_REPRESENTATION_ITEM ( )  RATIONAL_B_SPLINE_CURVE ( ( 1.000039740655109810, 0.9986931415022445302, 0.9997852197113853423, 1.003315975282531802, 1.003315975282531802, 1.003315975282531802, 1.003315975282531802, 1.003315975282531802, 1.003315975282531802, 0.9773170091682806815, 0.9773170091682806815, 1.003315975282531802, 1.003315975282531802, 1.003315975282531802, 1.003315975282531802, 1.003315975282531802, 1.003315975282531802, 0.9998573533027315108, 0.9987387818499366965, 0.9999602609241470264 ) ) 
 REPRESENTATION_ITEM ( '' )  );
#23871=CARTESIAN_POINT ( 'NONE',  ( 6.372119535971386917, -21.01724095701019479, -1.500000000000002220 ) ) ;
#23873=ORIENTED_EDGE ( 'NONE', *, *, #60048, .F. ) ;
#23875=EDGE_CURVE ( 'NONE', #60824, #41589, #88176, .T. ) ;
#23877=CARTESIAN_POINT ( 'NONE',  ( -0.6367455441941621830, -20.85161220577290919, 11.49999999999999645 ) ) ;
#23878=VECTOR ( 'NONE', #53346, 1000.000000000000114 ) ;
#23881=EDGE_CURVE ( 'NONE', #95349, #85527, #6917, .T. ) ;
#23882=CARTESIAN_POINT ( 'NONE',  ( -111.5562042904833930, -23.48786465467241769, 11.44779295918254292 ) ) ;
#23884=DIRECTION ( 'NONE',  ( -3.773278334453079030E-23, 0.9999999999976377785, 2.173523156925979128E-06 ) ) ;
#23885=CARTESIAN_POINT ( 'NONE',  ( 6.245503531335690361, -20.37428601906679759, 11.49999999999998934 ) ) ;
#23886=CARTESIAN_POINT ( 'NONE',  ( -98.51627056919916470, -23.96169478059713498, 10.65365249895717881 ) ) ;
#23887=ADVANCED_FACE ( 'NONE', ( #15607 ), #29338, .T. ) ;
#23888=CARTESIAN_POINT ( 'NONE',  ( -51.24168201688318902, -25.24975565039529002, 3.737730239075333749 ) ) ;
#23890=FACE_OUTER_BOUND ( 'NONE', #70666, .T. ) ;
#23891=CARTESIAN_POINT ( 'NONE',  ( -15.53634343318938704, 16.32316209468629253, -1.500000000000002220 ) ) ;
#23893=B_SPLINE_SURFACE_WITH_KNOTS ( 'NONE', 3, 1, ( 
 ( #14692, #22291 ),
 ( #45164, #46661 ),
 ( #85205, #68985 ),
 ( #8087, #99426 ),
 ( #39035, #23293 ),
 ( #76088, #69984 ),
 ( #62382, #29920 ),
 ( #70493, #30920 ),
 ( #38534, #54280 ),
 ( #15696, #61391 ),
 ( #92317, #16192 ),
 ( #39540, #31930 ),
 ( #45656, #76581 ),
 ( #93311, #976 ),
 ( #62899, #471 ),
 ( #84202, #15194 ),
 ( #55278, #92813 ),
 ( #7085, #93821 ),
 ( #22788, #78080 ) ),
 .UNSPECIFIED., .F., .F., .F.,
 ( 4, 1, 1, 1, 1, 1, 1, 1, 1, 1, 1, 1, 1, 1, 1, 1, 4 ),
 ( 2, 2 ),
 ( 0.000000000000000000, 0.07952482958501205790, 0.1550999763495347628, 0.2272198200732689910, 0.2959105041914696366, 0.3620558809471779993, 0.4255201169126350269, 0.4858127192253077209, 0.5444947060018110463, 0.6014596357222257161, 0.6578405937966476102, 0.7139744721931383653, 0.7694679515974504058, 0.8261299671813285839, 0.8828853593090686402, 0.9407008816662013606, 1.000000000000000000 ),
 ( 0.000000000000000000, 1.000000000000000000 ),
 .UNSPECIFIED. ) ;
#23894=CARTESIAN_POINT ( 'NONE',  ( -51.52287095715006870, -23.48786465467241058, 11.44779295918255002 ) ) ;
#23895=ORIENTED_EDGE ( 'NONE', *, *, #15983, .T. ) ;
#23898=CARTESIAN_POINT ( 'NONE',  ( -19.61143073682725202, -1.510137823221562092, 11.49999999999999645 ) ) ;
#23899=CARTESIAN_POINT ( 'NONE',  ( -28.62287095715003815, -23.58338348806757168, -1.053490783401417552 ) ) ;
#23900=CARTESIAN_POINT ( 'NONE',  ( -39.58953762381673158, -24.64898659630366851, 1.056161002820378281 ) ) ;
#23901=B_SPLINE_CURVE_WITH_KNOTS ( 'NONE', 3,
 ( #52031, #52526, #75847, #29682 ),
 .UNSPECIFIED., .F., .F.,
 ( 4, 4 ),
 ( 0.000000000000000000, 9.999999999997510880E-05 ),
 .UNSPECIFIED. ) ;
#23902=EDGE_CURVE ( 'NONE', #62329, #53678, #68902, .T. ) ;
#23903=VERTEX_POINT ( 'NONE', #38451 ) ;
#23904=CARTESIAN_POINT ( 'NONE',  ( -99.59615587936018244, -23.73766607897671577, -1.055555164236429144 ) ) ;
#23906=CARTESIAN_POINT ( 'NONE',  ( -90.93339583912592161, -25.25787539255926362, 3.590294762828090125 ) ) ;
#23908=CARTESIAN_POINT ( 'NONE',  ( -70.70074709382635092, -25.25639587447663459, 7.037036448897811880 ) ) ;
#23909=CARTESIAN_POINT ( 'NONE',  ( 12.09797951242163805, 15.59582292391970704, -1.500000000000002220 ) ) ;
#23910=ORIENTED_EDGE ( 'NONE', *, *, #35351, .T. ) ;
#23916=CARTESIAN_POINT ( 'NONE',  ( -80.62287095715005592, -24.99132157543084531, 2.256160258750667502 ) ) ;
#23917=CARTESIAN_POINT ( 'NONE',  ( -69.37717373815038968, -25.26785222005164400, 5.961561438218058839 ) ) ;
#23918=CARTESIAN_POINT ( 'NONE',  ( -99.83839741074528717, -25.03145156749568656, 7.461409701454681631 ) ) ;
#23922=CARTESIAN_POINT ( 'NONE',  ( -112.5228709571500616, -23.47596703998600631, 11.44779298504228038 ) ) ;
#23923=CARTESIAN_POINT ( 'NONE',  ( -10.28607412905329532, -17.16720287211733975, -1.500000000000002220 ) ) ;
#23924=B_SPLINE_CURVE_WITH_KNOTS ( 'NONE', 3,
 ( #43281, #67124, #35166, #42301, #26553, #81830 ),
 .UNSPECIFIED., .F., .F.,
 ( 4, 2, 4 ),
 ( 0.000000000000000000, 0.001380764517853249902, 0.002761529035706499803 ),
 .UNSPECIFIED. ) ;
#23926=CARTESIAN_POINT ( 'NONE',  ( -99.13021050592293193, -25.27533083522742174, 3.853444758578534302 ) ) ;
#23927=CARTESIAN_POINT ( 'NONE',  ( -116.6235094140349560, -24.66019654487199730, 8.947790411086115725 ) ) ;
#23929=EDGE_CURVE ( 'NONE', #51268, #23352, #55460, .T. ) ;
#23930=CARTESIAN_POINT ( 'NONE',  ( -79.62973378576782579, -24.35071581493543036, 9.817618358456028815 ) ) ;
#23931=CARTESIAN_POINT ( 'NONE',  ( -109.9559143002945234, -25.29012739791637188, 3.359997386848465606 ) ) ;
#23932=FACE_OUTER_BOUND ( 'NONE', #36982, .T. ) ;
#23934=DIRECTION ( 'NONE',  ( 0.000000000000000000, -0.9999999999976377785, -2.173523156925979975E-06 ) ) ;
#23936=DIRECTION ( 'NONE',  ( 0.000000000000000000, -2.173523156925979552E-06, 0.9999999999976378895 ) ) ;
#23937=EDGE_CURVE ( 'NONE', #99569, #57091, #53694, .T. ) ;
#23940=CARTESIAN_POINT ( 'NONE',  ( -8.348131891436525009, -18.51812344263101906, -1.500000000000002220 ) ) ;
#23941=EDGE_CURVE ( 'NONE', #38564, #19712, #45746, .T. ) ;
#23942=CARTESIAN_POINT ( 'NONE',  ( -28.58953762381673513, -24.50408623682959686, 1.056161642721338279 ) ) ;
#23944=CARTESIAN_POINT ( 'NONE',  ( -40.02662038540177747, -25.27394419400966541, 6.217212794464101577 ) ) ;
#23946=LINE ( 'NONE', #615, #16145 ) ;
#23947=CARTESIAN_POINT ( 'NONE',  ( -18.82377384687745447, 7.257840063761761051, -1.500000000000002220 ) ) ;
#23948=CARTESIAN_POINT ( 'NONE',  ( 16.66693084842116335, 13.01107939256401913, 11.49999999999999645 ) ) ;
#23949=CARTESIAN_POINT ( 'NONE',  ( -22.05048665130746954, -1.834114841651104832, -1.500000000000002220 ) ) ;
#23951=CARTESIAN_POINT ( 'NONE',  ( 15.43701773751798001, -13.56989305476470875, -1.500000000000002220 ) ) ;
#23952=CARTESIAN_POINT ( 'NONE',  ( -60.58332302833671434, -24.73486907724917572, 1.287355809206962798 ) ) ;
#23953=ORIENTED_EDGE ( 'NONE', *, *, #9579, .T. ) ;
#23954=CARTESIAN_POINT ( 'NONE',  ( -32.62287095715004170, -24.50216790748204687, 0.6166512839542539481 ) ) ;
#23956=CARTESIAN_POINT ( 'NONE',  ( -51.62287095715007013, -23.72747288104469732, -1.053458166803226792 ) ) ;
#23957=CARTESIAN_POINT ( 'NONE',  ( -70.62287095715005592, -24.99132157543083821, 2.256160258750667502 ) ) ;
#23959=ORIENTED_EDGE ( 'NONE', *, *, #68767, .T. ) ;
#23960=EDGE_LOOP ( 'NONE', ( #49449, #99307, #13976, #17202 ) ) ;
#23961=CARTESIAN_POINT ( 'NONE',  ( -103.5895376238167245, -23.48786465467241769, 11.44779295918254114 ) ) ;
#23963=CARTESIAN_POINT ( 'NONE',  ( -68.56536383884358088, -23.48786465467241058, 11.44779295918254824 ) ) ;
#23964=CARTESIAN_POINT ( 'NONE',  ( 6.296002175621457475, 19.65409743616946514, -1.500000000000002220 ) ) ;
#23965=CARTESIAN_POINT ( 'NONE',  ( 11.61936018155104833, -18.21891831228114356, 11.49999999999999645 ) ) ;
#23967=DIRECTION ( 'NONE',  ( -3.773278334444166432E-23, 1.000000000000000000, 0.000000000000000000 ) ) ;
#23969=CARTESIAN_POINT ( 'NONE',  ( -4.763361739610138201, -21.85411462188651299, -1.500000000000002220 ) ) ;
#23971=CARTESIAN_POINT ( 'NONE',  ( -79.35008398046767297, -25.12205589522605109, 6.078937818662843107 ) ) ;
#23972=CARTESIAN_POINT ( 'NONE',  ( -120.6228709571499991, -24.62285846362215835, 9.038163152653522658 ) ) ;
#23973=ORIENTED_EDGE ( 'NONE', *, *, #23422, .F. ) ;
#23974=CARTESIAN_POINT ( 'NONE',  ( -99.72456502726817007, -25.30354620733853821, 4.451988771325939176 ) ) ;
#23975=CARTESIAN_POINT ( 'NONE',  ( -60.52287095715006160, -23.47596703998600631, 11.44779298504228926 ) ) ;
#23976=CARTESIAN_POINT ( 'NONE',  ( -11.35812032211249090, 17.58211214940072864, 11.49999999999998934 ) ) ;
#23977=EDGE_LOOP ( 'NONE', ( #33580, #76263, #61371, #43453 ) ) ;
#23978=CARTESIAN_POINT ( 'NONE',  ( -87.58953762381668184, -23.48786465467241769, 11.44779295918254114 ) ) ;
#23979=VECTOR ( 'NONE', #58447, 1000.000000000000114 ) ;
#23981=CARTESIAN_POINT ( 'NONE',  ( -50.62287095715004881, -24.14406661707768365, 10.28769366152060449 ) ) ;
#23982=CARTESIAN_POINT ( 'NONE',  ( 12.34367313097222763, -17.18290682204727915, -1.500000000000002220 ) ) ;
#23983=ORIENTED_EDGE ( 'NONE', *, *, #21737, .F. ) ;
#23984=FACE_OUTER_BOUND ( 'NONE', #32432, .T. ) ;
#23985=CARTESIAN_POINT ( 'NONE',  ( -21.80608713477256089, -0.9339522974687717305, -1.500000000000002220 ) ) ;
#23988=B_SPLINE_CURVE_WITH_KNOTS ( 'NONE', 3,
 ( #92606, #82997, #37347, #84503 ),
 .UNSPECIFIED., .F., .F.,
 ( 4, 4 ),
 ( 0.000000000000000000, 0.001530649038461562306 ),
 .UNSPECIFIED. ) ;
#23989=CARTESIAN_POINT ( 'NONE',  ( -107.5228709571501184, -23.72747288104470442, -1.053458166803225460 ) ) ;
#23990=B_SPLINE_CURVE_WITH_KNOTS ( 'NONE', 3,
 ( #95880, #57346, #88279, #18748 ),
 .UNSPECIFIED., .F., .F.,
 ( 4, 4 ),
 ( 0.5802002312608413037, 0.5892066625329569485 ),
 .UNSPECIFIED. ) ;
#23991=CARTESIAN_POINT ( 'NONE',  ( -116.6228709571501412, -23.96127896941633750, -0.6493128931037774887 ) ) ;
#23992=CARTESIAN_POINT ( 'NONE',  ( 4.771108217193557266, 21.26182814020628697, -1.500000000000002220 ) ) ;
#23994=ADVANCED_FACE ( 'NONE', ( #37950 ), #31338, .T. ) ;
#23995=ORIENTED_EDGE ( 'NONE', *, *, #85544, .T. ) ;
#23997=CARTESIAN_POINT ( 'NONE',  ( -85.54292597230013939, -24.73531770709095312, 8.716586749053508498 ) ) ;
#23999=ORIENTED_EDGE ( 'NONE', *, *, #71105, .T. ) ;
#24002=EDGE_CURVE ( 'NONE', #125, #84745, #100323, .T. ) ;
#24004=CARTESIAN_POINT ( 'NONE',  ( -31.24388727629347784, -24.87479601683088148, 8.247789944647559324 ) ) ;
#24005=CARTESIAN_POINT ( 'NONE',  ( 19.38521227897113874, -8.589346653930519437, 11.49999999999998934 ) ) ;
#24008=CARTESIAN_POINT ( 'NONE',  ( -79.98156793206884174, -25.03138283009880283, 7.487049201991271552 ) ) ;
#24011=CARTESIAN_POINT ( 'NONE',  ( 19.38287969867323213, 0.6573286442255052986, -1.500000000000002220 ) ) ;
#24012=CARTESIAN_POINT ( 'NONE',  ( -39.02904432526693768, -25.20650829394578096, 6.812666491500988464 ) ) ;
#24013=ORIENTED_EDGE ( 'NONE', *, *, #81249, .T. ) ;
#24014=CARTESIAN_POINT ( 'NONE',  ( 13.74000504945409418, 13.82049530813991467, 11.49999999999999645 ) ) ;
#24016=CARTESIAN_POINT ( 'NONE',  ( -108.6228709571500701, -23.48783264082478794, -1.443836473390060604 ) ) ;
#24017=EDGE_CURVE ( 'NONE', #79371, #18949, #16624, .T. ) ;
#24019=CARTESIAN_POINT ( 'NONE',  ( -103.5228709571500758, -23.47596703998600631, 11.44779298504228215 ) ) ;
#24021=CARTESIAN_POINT ( 'NONE',  ( -103.5562042904834072, -23.47593901973091235, -1.443836447539001089 ) ) ;
#24022=CARTESIAN_POINT ( 'NONE',  ( -93.63360700857630547, -23.96169478059713498, 10.65365249895717170 ) ) ;
#24023=CARTESIAN_POINT ( 'NONE',  ( -6.620539020842763911, -18.51205181221761720, 11.49999999999998934 ) ) ;
#24024=B_SPLINE_CURVE_WITH_KNOTS ( 'NONE', 3,
 ( #98426, #29926, #83208, #13694 ),
 .UNSPECIFIED., .F., .F.,
 ( 4, 4 ),
 ( 0.000000000000000000, 0.0001002978966067898494 ),
 .UNSPECIFIED. ) ;
#24025=B_SPLINE_SURFACE_WITH_KNOTS ( 'NONE', 3, 1, ( 
 ( #97011, #74177 ),
 ( #36113, #3677 ),
 ( #26510, #4673 ),
 ( #65594, #97992 ),
 ( #28492, #88407 ),
 ( #59454, #65096 ),
 ( #90399, #28003 ),
 ( #35622, #66596 ),
 ( #58960, #20874 ),
 ( #51845, #81288 ),
 ( #82778, #11772 ),
 ( #73678, #13260 ),
 ( #34124, #18882 ),
 ( #27512, #57972 ),
 ( #19874, #50849 ),
 ( #81788, #68068 ),
 ( #30488, #76646 ),
 ( #84773, #52836 ),
 ( #99491, #59964 ) ),
 .UNSPECIFIED., .F., .F., .F.,
 ( 4, 1, 1, 1, 1, 1, 1, 1, 1, 1, 1, 1, 1, 1, 1, 1, 4 ),
 ( 2, 2 ),
 ( 0.000000000000000000, 0.06871184072392559627, 0.1348120656080472046, 0.1995375926079888951, 0.2633349351079785627, 0.3267474805653824976, 0.3903284830692779206, 0.4541258255692630641, 0.5192033216913150007, 0.5835101452921214182, 0.6454971827645034077, 0.7052898423114491999, 0.7634875795843552027, 0.8218564001280685982, 0.8800042732065155304, 0.9391077098979025983, 1.000000000000000000 ),
 ( 0.000000000000000000, 1.000000000000000000 ),
 .UNSPECIFIED. ) ;
#24026=CARTESIAN_POINT ( 'NONE',  ( -41.44897309030830712, -25.31583615692164102, 4.366647674295371928 ) ) ;
#24027=EDGE_LOOP ( 'NONE', ( #8634, #71669, #81226, #13117 ) ) ;
#24028=CARTESIAN_POINT ( 'NONE',  ( -13.01863397230089170, 17.21462230531794901, -1.500000000000002220 ) ) ;
#24029=CARTESIAN_POINT ( 'NONE',  ( -40.47472236188045258, -24.83618233451449342, 1.606449574219539711 ) ) ;
#24031=CARTESIAN_POINT ( 'NONE',  ( 3.535601659403828201, -22.84449096179584160, -1.500000000000002220 ) ) ;
#24033=DIRECTION ( 'NONE',  ( -1.000000000000000000, -3.773278334444167608E-23, -8.201307833595939069E-29 ) ) ;
#24035=CARTESIAN_POINT ( 'NONE',  ( -42.62287095715004881, -23.47593901973091235, -1.443836447539011525 ) ) ;
#24036=CARTESIAN_POINT ( 'NONE',  ( -120.5228709571500616, -23.48786465467241769, 11.44779295918253759 ) ) ;
#24037=CARTESIAN_POINT ( 'NONE',  ( -109.7472523716161419, -25.20850093776611089, 3.466865132916900460 ) ) ;
#24038=CARTESIAN_POINT ( 'NONE',  ( -129.5898459675138952, -23.96119346886881019, -0.6495511937831975890 ) ) ;
#24039=CARTESIAN_POINT ( 'NONE',  ( -114.6235148883246637, -24.66019654487200441, 8.947790411086106843 ) ) ;
#24040=CARTESIAN_POINT ( 'NONE',  ( -15.73602684802347440, -12.20685706852216867, 11.49999999999998934 ) ) ;
#24042=CARTESIAN_POINT ( 'NONE',  ( -9.893332137849947472, -17.22304987741864579, -1.500000000000002220 ) ) ;
#24044=CARTESIAN_POINT ( 'NONE',  ( -32.62287095715006302, -23.47596703998600276, 11.44779298504227505 ) ) ;
#24045=EDGE_CURVE ( 'NONE', #85108, #2769, #98930, .T. ) ;
#24046=CARTESIAN_POINT ( 'NONE',  ( -39.22373867983765194, -25.10925741625206342, 3.518977594474388848 ) ) ;
#24048=CARTESIAN_POINT ( 'NONE',  ( 10.28901978357889035, -18.02705789925236957, 11.49999999999999645 ) ) ;
#24049=FACE_OUTER_BOUND ( 'NONE', #17260, .T. ) ;
#24050=EDGE_CURVE ( 'NONE', #59175, #64167, #29923, .T. ) ;
#24051=FACE_OUTER_BOUND ( 'NONE', #63050, .T. ) ;
#24052=CARTESIAN_POINT ( 'NONE',  ( 0.9741843557120299923, -22.74547949729550922, 11.49999999999999645 ) ) ;
#24054=ORIENTED_EDGE ( 'NONE', *, *, #92093, .T. ) ;
#24055=CARTESIAN_POINT ( 'NONE',  ( -32.62287095715004881, -29.50247984919015209, -1.443849546365062242 ) ) ;
#24059=CARTESIAN_POINT ( 'NONE',  ( -20.17641613807547785, 1.360797614858565874, 11.49999999999998934 ) ) ;
#24060=CARTESIAN_POINT ( 'NONE',  ( -56.62287095715005592, -29.50250786944525672, 11.44777988621623876 ) ) ;
#24061=LINE ( 'NONE', #94076, #52844 ) ;
#24062=B_SPLINE_CURVE_WITH_KNOTS ( 'NONE', 3,
 ( #51286, #35567, #96957, #97457 ),
 .UNSPECIFIED., .F., .F.,
 ( 4, 4 ),
 ( 0.000000000000000000, 9.999999999998897304E-05 ),
 .UNSPECIFIED. ) ;
#24066=CARTESIAN_POINT ( 'NONE',  ( -2.941484630304247450, -22.72858670154147376, -1.500000000000002220 ) ) ;
#24067=CARTESIAN_POINT ( 'NONE',  ( -40.43756433397305017, -25.12049752546737835, 2.832404795212222659 ) ) ;
#24068=CARTESIAN_POINT ( 'NONE',  ( -18.67883320684159543, -10.89015303950203517, -1.500000000000002220 ) ) ;
#24070=FACE_OUTER_BOUND ( 'NONE', #15549, .T. ) ;
#24071=CARTESIAN_POINT ( 'NONE',  ( -18.73635099073748833, 9.434554061794083069, 11.49999999999999645 ) ) ;
#24072=ORIENTED_EDGE ( 'NONE', *, *, #38333, .T. ) ;
#24074=CARTESIAN_POINT ( 'NONE',  ( -124.5891633685761803, -24.51314013834316086, 0.6176544820404203939 ) ) ;
#24075=CARTESIAN_POINT ( 'NONE',  ( 9.413913215453616701, -19.89622248225912315, 11.49999999999998934 ) ) ;
#24076=ADVANCED_FACE ( 'NONE', ( #55699 ), #8506, .T. ) ;
#24078=ORIENTED_EDGE ( 'NONE', *, *, #3223, .F. ) ;
#24079=CARTESIAN_POINT ( 'NONE',  ( -49.73776537321236901, -25.18440148854909921, 3.509878368039943464 ) ) ;
#24081=VERTEX_POINT ( 'NONE', #32846 ) ;
#24083=ORIENTED_EDGE ( 'NONE', *, *, #24245, .T. ) ;
#24088=CARTESIAN_POINT ( 'NONE',  ( 13.31029742451639386, -15.53102932315203510, -1.500000000000002220 ) ) ;
#24090=CARTESIAN_POINT ( 'NONE',  ( -100.6814946224345846, -25.30401792888237367, 5.197789011716578145 ) ) ;
#24091=EDGE_CURVE ( 'NONE', #73894, #59704, #70407, .T. ) ;
#24092=CARTESIAN_POINT ( 'NONE',  ( -33.62287095715005592, -24.66019654487199020, 8.947790411086138818 ) ) ;
#24094=CARTESIAN_POINT ( 'NONE',  ( -20.55991158545366204, 8.586518200734140294, 11.49999999999998934 ) ) ;
#24095=EDGE_CURVE ( 'NONE', #80512, #43640, #85643, .T. ) ;
#24096=CARTESIAN_POINT ( 'NONE',  ( -71.30292240304103757, -25.24939213713761887, 6.271475255338955002 ) ) ;
#24097=CARTESIAN_POINT ( 'NONE',  ( -26.01933804882074597, -24.74254525576054320, 7.260434932203454039 ) ) ;
#24101=EDGE_CURVE ( 'NONE', #8769, #20357, #4610, .T. ) ;
#24102=CARTESIAN_POINT ( 'NONE',  ( -20.74012505511919713, -1.853331690952414013, 11.49999999999998934 ) ) ;
#24105=ORIENTED_EDGE ( 'NONE', *, *, #34229, .T. ) ;
#24107=CARTESIAN_POINT ( 'NONE',  ( -51.49483116284216067, -25.25854422715338288, 6.426654113949027192 ) ) ;
#24108=CARTESIAN_POINT ( 'NONE',  ( 3.785439364192078937, -20.66625369722972749, -1.500000000000002220 ) ) ;
#24109=ORIENTED_EDGE ( 'NONE', *, *, #74914, .T. ) ;
#24110=DIRECTION ( 'NONE',  ( -3.773278334453079618E-23, 0.9999999999976377785, 2.173523156925979975E-06 ) ) ;
#24112=CARTESIAN_POINT ( 'NONE',  ( -32.52287095715006160, -29.50248528299804818, 1.056150453629029817 ) ) ;
#24115=CARTESIAN_POINT ( 'NONE',  ( -40.62287095715004881, -24.52323809116983355, 9.355190652339421931 ) ) ;
#24116=CARTESIAN_POINT ( 'NONE',  ( -49.58953762381673869, -24.64898659630528499, 1.056161002820820372 ) ) ;
#24117=CARTESIAN_POINT ( 'NONE',  ( -64.52287095715006160, -24.64965694238407323, 8.947790433994201820 ) ) ;
#24118=ADVANCED_FACE ( 'NONE', ( #33333 ), #25729, .F. ) ;
#24119=CARTESIAN_POINT ( 'NONE',  ( -20.56242917251232782, -8.299981740788712870, 11.49999999999999645 ) ) ;
#24124=CARTESIAN_POINT ( 'NONE',  ( -7.311831771877058905, -21.45741656709679646, -1.500000000000002220 ) ) ;
#24127=ORIENTED_EDGE ( 'NONE', *, *, #24224, .F. ) ;
#24128=ORIENTED_EDGE ( 'NONE', *, *, #73256, .T. ) ;
#24131=CARTESIAN_POINT ( 'NONE',  ( 18.82035724208558491, -7.196742317222773799, 11.49999999999998934 ) ) ;
#24132=EDGE_CURVE ( 'NONE', #19712, #7766, #34789, .T. ) ;
#24133=DIRECTION ( 'NONE',  ( 0.000000000000000000, -0.9999999999976377785, -2.173523156925979975E-06 ) ) ;
#24136=DIRECTION ( 'NONE',  ( 1.000000000000000000, 3.773278334444167608E-23, 8.201307833595939069E-29 ) ) ;
#24137=CARTESIAN_POINT ( 'NONE',  ( 6.497064355747536268, 21.42967291005575348, -1.500000000000002220 ) ) ;
#24138=ADVANCED_FACE ( 'NONE', ( #94735 ), #95742, .F. ) ;
#24139=ORIENTED_EDGE ( 'NONE', *, *, #51871, .F. ) ;
#24143=CARTESIAN_POINT ( 'NONE',  ( -39.64491860520665512, -25.31344806528496250, 4.759838987950200995 ) ) ;
#24144=PLANE ( 'NONE',  #98414 ) ;
#24145=EDGE_CURVE ( 'NONE', #62281, #47994, #94073, .T. ) ;
#24147=CARTESIAN_POINT ( 'NONE',  ( -18.05301863641116000, -7.546005365994440162, -1.500000000000002220 ) ) ;
#24149=ORIENTED_EDGE ( 'NONE', *, *, #84369, .T. ) ;
#24150=CARTESIAN_POINT ( 'NONE',  ( 5.543860000110784725, 20.76261553274053284, 11.49999999999998934 ) ) ;
#24151=DIRECTION ( 'NONE',  ( 0.000000000000000000, -0.9999999999976377785, -2.173523156925979128E-06 ) ) ;
#24152=CARTESIAN_POINT ( 'NONE',  ( -38.52287095715006870, -23.47593901973090169, -1.443836447538997092 ) ) ;
#24154=FACE_OUTER_BOUND ( 'NONE', #63975, .T. ) ;
#24155=CARTESIAN_POINT ( 'NONE',  ( -22.87863416751641310, 0.2071024363326711970, -1.500000000000002220 ) ) ;
#24156=VECTOR ( 'NONE', #85059, 1000.000000000000227 ) ;
#24158=FACE_OUTER_BOUND ( 'NONE', #36305, .T. ) ;
#24160=CARTESIAN_POINT ( 'NONE',  ( -10.14125802585430947, 17.27231531754821603, 11.49999999999999645 ) ) ;
#24161=CARTESIAN_POINT ( 'NONE',  ( -79.44434589896187049, -25.31594384477702775, 4.820847139809496085 ) ) ;
#24164=CARTESIAN_POINT ( 'NONE',  ( -103.5228709571500758, -24.64898659630367916, 1.056161002820829697 ) ) ;
#24165=ORIENTED_EDGE ( 'NONE', *, *, #31083, .F. ) ;
#24167=CARTESIAN_POINT ( 'NONE',  ( 5.219777686717518961, -21.12652377152128480, -1.500000000000002220 ) ) ;
#24169=CARTESIAN_POINT ( 'NONE',  ( -19.44079195400435012, 3.002763184081948200, -1.500000000000002220 ) ) ;
#24170=CARTESIAN_POINT ( 'NONE',  ( -122.6228709571500559, -23.73907113216991860, -1.053371485793221485 ) ) ;
#24171=ADVANCED_FACE ( 'NONE', ( #49085 ), #80015, .F. ) ;
#24172=CARTESIAN_POINT ( 'NONE',  ( -104.5228709571500758, -23.48786465467241769, 11.44779295918254114 ) ) ;
#24174=CARTESIAN_POINT ( 'NONE',  ( -56.62287095715007013, -24.33927499327855060, 9.819080762295818943 ) ) ;
#24176=CARTESIAN_POINT ( 'NONE',  ( 16.23509277041898358, 12.58620111108425377, 11.49999999999999645 ) ) ;
#24178=CARTESIAN_POINT ( 'NONE',  ( -75.62287095715004170, -29.50248789122583659, 2.256150453626215580 ) ) ;
#24179=CARTESIAN_POINT ( 'NONE',  ( -21.83012794225054165, -5.757306806698124113, 11.49999999999999645 ) ) ;
#24180=EDGE_CURVE ( 'NONE', #96748, #73682, #73904, .T. ) ;
#24181=EDGE_LOOP ( 'NONE', ( #19575, #53482, #97470, #2407 ) ) ;
#24182=CARTESIAN_POINT ( 'NONE',  ( -70.12829555472771403, -25.12219141572935044, 7.087033598080036079 ) ) ;
#24183=CARTESIAN_POINT ( 'NONE',  ( -27.60893876761982213, -24.80447294267062830, 7.602474626589142304 ) ) ;
#24184=CARTESIAN_POINT ( 'NONE',  ( -125.6240011470757025, -24.73531770709095312, 8.716586749053508498 ) ) ;
#24185=CARTESIAN_POINT ( 'NONE',  ( -69.58953762381671027, -24.64965694238407323, 8.947790433994656567 ) ) ;
#24186=B_SPLINE_CURVE_WITH_KNOTS ( 'NONE', 3,
 ( #81425, #19514, #88540, #43372 ),
 .UNSPECIFIED., .F., .F.,
 ( 4, 4 ),
 ( 0.2299501262341301644, 0.2389565575062454206 ),
 .UNSPECIFIED. ) ;
#24188=CARTESIAN_POINT ( 'NONE',  ( -125.5562042904834215, -23.47596703998600631, 11.44779298504227683 ) ) ;
#24189=AXIS2_PLACEMENT_3D ( 'NONE', #29592, #75760, #74281 ) ;
#24190=ORIENTED_EDGE ( 'NONE', *, *, #26294, .F. ) ;
#24191=CARTESIAN_POINT ( 'NONE',  ( -79.80213995901898727, -25.26749909610970235, 5.120505659559028366 ) ) ;
#24192=CARTESIAN_POINT ( 'NONE',  ( 22.73759373355791169, -1.750760473330008171, -1.500000000000002220 ) ) ;
#24194=AXIS2_PLACEMENT_3D ( 'NONE', #81510, #50555, #13477 ) ;
#24195=CARTESIAN_POINT ( 'NONE',  ( -115.5228709571501042, -24.51254535375846899, 9.355368624242137443 ) ) ;
#24196=CARTESIAN_POINT ( 'NONE',  ( -59.66801233241169911, -25.31912262272984293, 4.489962371710368494 ) ) ;
#24197=CARTESIAN_POINT ( 'NONE',  ( -3.217810451210200817, -22.18463865543611391, 11.49999999999999645 ) ) ;
#24201=CARTESIAN_POINT ( 'NONE',  ( -12.46176837856299002, 18.05058065364367792, -1.500000000000002220 ) ) ;
#24204=AXIS2_PLACEMENT_3D ( 'NONE', #33005, #32499, #62964 ) ;
#24205=CARTESIAN_POINT ( 'NONE',  ( -110.5895376238167245, -25.00158670708909625, 2.256160236439165523 ) ) ;
#24206=CARTESIAN_POINT ( 'NONE',  ( -74.55620429048340725, -23.48786465467241058, 11.44779295918255002 ) ) ;
#24207=ORIENTED_EDGE ( 'NONE', *, *, #41645, .T. ) ;
#24209=CARTESIAN_POINT ( 'NONE',  ( -42.62287095715004881, -29.50247984919015209, -1.443849546365060466 ) ) ;
#24211=CARTESIAN_POINT ( 'NONE',  ( -16.48689143942861079, 12.14541645011370541, -1.500000000000002220 ) ) ;
#24216=CARTESIAN_POINT ( 'NONE',  ( 16.10802587768190008, -16.50329280669357246, 11.49999999999998934 ) ) ;
#24217=CARTESIAN_POINT ( 'NONE',  ( -49.10797093729408402, -25.26756514004985377, 3.919560524017612124 ) ) ;
#24218=CARTESIAN_POINT ( 'NONE',  ( -2.359408512905806443, -20.17289352931189583, -1.500000000000002220 ) ) ;
#24219=ORIENTED_EDGE ( 'NONE', *, *, #84409, .T. ) ;
#24220=ADVANCED_FACE ( 'NONE', ( #59186 ), #79017, .T. ) ;
#24223=CARTESIAN_POINT ( 'NONE',  ( -92.55185405631918627, -24.15543982623908192, -0.2315651400026453588 ) ) ;
#24224=EDGE_CURVE ( 'NONE', #11368, #87961, #11771, .T. ) ;
#24225=CARTESIAN_POINT ( 'NONE',  ( -93.62287095715007013, -23.47596703998600631, 11.44779298504227860 ) ) ;
#24226=CARTESIAN_POINT ( 'NONE',  ( -70.53413262234137449, -24.92564183028979130, 1.928384488918253536 ) ) ;
#24227=CARTESIAN_POINT ( 'NONE',  ( 0.6623178260406717976, 21.47796536025111536, 11.49999999999999645 ) ) ;
#24230=CARTESIAN_POINT ( 'NONE',  ( -61.52208231706953967, -23.48786465467240703, 11.44779295918255002 ) ) ;
#24231=EDGE_CURVE ( 'NONE', #63074, #13848, #44494, .T. ) ;
#24232=ORIENTED_EDGE ( 'NONE', *, *, #52915, .T. ) ;
#24233=CARTESIAN_POINT ( 'NONE',  ( 20.09396958936853395, 5.161349618257207617, -1.500000000000002220 ) ) ;
#24234=ORIENTED_EDGE ( 'NONE', *, *, #99711, .F. ) ;
#24235=CARTESIAN_POINT ( 'NONE',  ( -125.5198031208248324, -24.73486907724918638, 1.287355809206972346 ) ) ;
#24237=CARTESIAN_POINT ( 'NONE',  ( -75.62287095715007013, -24.14406661707769075, 10.28769366152060982 ) ) ;
#24241=CARTESIAN_POINT ( 'NONE',  ( -101.6228709571500559, -29.50250243563736774, 8.947779886222138046 ) ) ;
#24242=CARTESIAN_POINT ( 'NONE',  ( -42.58141094947423966, -24.51419770103158413, 9.386484678747191168 ) ) ;
#24243=CARTESIAN_POINT ( 'NONE',  ( -28.07518484056776131, -24.65329974738956409, 1.661544776103349941 ) ) ;
#24244=ADVANCED_FACE ( 'NONE', ( #66814 ), #30718, .T. ) ;
#24245=EDGE_CURVE ( 'NONE', #79008, #74917, #23988, .T. ) ;
#24246=CARTESIAN_POINT ( 'NONE',  ( 21.84380375219137349, -3.031640915038902762, 11.49999999999999645 ) ) ;
#24247=CARTESIAN_POINT ( 'NONE',  ( -89.50836770226504768, -24.35071581493543391, 9.817618358456025263 ) ) ;
#24248=CARTESIAN_POINT ( 'NONE',  ( -3.174168706971715270, 22.36591850054903929, 11.49999999999998934 ) ) ;
#24249=CARTESIAN_POINT ( 'NONE',  ( 19.54352652498339182, 7.673529024697476331, -1.500000000000002220 ) ) ;
#24250=CARTESIAN_POINT ( 'NONE',  ( -105.6228709571500559, -23.47593901973091235, -1.443836447538999312 ) ) ;
#24251=PLANE ( 'NONE',  #2069 ) ;
#24252=VERTEX_POINT ( 'NONE', #38825 ) ;
#24253=ORIENTED_EDGE ( 'NONE', *, *, #10527, .F. ) ;
#24259=CARTESIAN_POINT ( 'NONE',  ( 20.71511372717374755, 4.256074106246791722, 11.49999999999998934 ) ) ;
#24260=CARTESIAN_POINT ( 'NONE',  ( -82.62287095715007013, -23.73907113216990794, -1.053371485793227924 ) ) ;
#24261=CARTESIAN_POINT ( 'NONE',  ( -61.66375751369396596, -25.20144863547804803, 6.835696751361012957 ) ) ;
#24262=VECTOR ( 'NONE', #74391, 1000.000000000000114 ) ;
#24263=DIRECTION ( 'NONE',  ( 3.773278334444167608E-23, -1.000000000000000000, 0.000000000000000000 ) ) ;
#24264=CARTESIAN_POINT ( 'NONE',  ( -89.81226385320383088, -29.50249591506787894, 5.947779886229223045 ) ) ;
#24266=CARTESIAN_POINT ( 'NONE',  ( -18.13406196532287140, 12.77545654309102474, -1.500000000000002220 ) ) ;
#24267=CARTESIAN_POINT ( 'NONE',  ( -81.63689878905805131, -23.96169478059713498, 10.65365249895718591 ) ) ;
#24269=ORIENTED_EDGE ( 'NONE', *, *, #32284, .F. ) ;
#24271=CARTESIAN_POINT ( 'NONE',  ( -48.62287095715004881, -24.64898659630528144, 1.056161002820821038 ) ) ;
#24272=CARTESIAN_POINT ( 'NONE',  ( -40.17542836734610745, -25.30419542993397641, 5.528894015552427099 ) ) ;
#24273=B_SPLINE_CURVE_WITH_KNOTS ( 'NONE', 3,
 ( #97696, #83461, #51536, #21061 ),
 .UNSPECIFIED., .F., .F.,
 ( 4, 4 ),
 ( 0.000000000000000000, 1.000000000000000000 ),
 .UNSPECIFIED. ) ;
#24276=CARTESIAN_POINT ( 'NONE',  ( -100.5461034797779547, -24.83618233451451118, 1.606449574219533050 ) ) ;
#24277=PLANE ( 'NONE',  #98774 ) ;
#24280=CARTESIAN_POINT ( 'NONE',  ( 19.32586673001642197, -2.567307930040524599, -1.500000000000002220 ) ) ;
#24281=VECTOR ( 'NONE', #23409, 1000.000000000000114 ) ;
#24282=CARTESIAN_POINT ( 'NONE',  ( -8.434714792116727367, -19.68496499552307455, -1.500000000000002220 ) ) ;
#24283=CARTESIAN_POINT ( 'NONE',  ( -62.53525840560303095, -24.65952944569303895, 1.056160979905693686 ) ) ;
#24285=CARTESIAN_POINT ( 'NONE',  ( -51.61379554000202319, -23.48783264082476308, -1.443836473390094133 ) ) ;
#24286=CARTESIAN_POINT ( 'NONE',  ( -101.1478676400630405, -25.18440077821660239, 3.600571543962751253 ) ) ;
#24287=CARTESIAN_POINT ( 'NONE',  ( -21.16080155796574047, 8.166215375980355518, -1.500000000000002220 ) ) ;
#24291=CARTESIAN_POINT ( 'NONE',  ( 19.41305359857673096, 4.112862643401165919, 11.49999999999999645 ) ) ;
#24294=LINE ( 'NONE', #80080, #60270 ) ;
#24297=PLANE ( 'NONE',  #66948 ) ;
#24298=CARTESIAN_POINT ( 'NONE',  ( -37.62287095715006302, -24.65952944569304250, 1.056160979905693020 ) ) ;
#24299=CARTESIAN_POINT ( 'NONE',  ( -15.83346750871019992, -14.79491179806518630, 11.49999999999998934 ) ) ;
#24300=CARTESIAN_POINT ( 'NONE',  ( -56.58743753624276707, -24.35071581493543391, 9.817618358456030592 ) ) ;
#24301=CARTESIAN_POINT ( 'NONE',  ( -14.69715086760845857, -12.76062437926726290, -1.500000000000002220 ) ) ;
#24302=CARTESIAN_POINT ( 'NONE',  ( -61.62287095715004881, -23.48786465467240347, 11.44779295918254824 ) ) ;
#24304=CARTESIAN_POINT ( 'NONE',  ( 17.64890103348723116, 10.21726211432410203, 11.49999999999999645 ) ) ;
#24306=FACE_OUTER_BOUND ( 'NONE', #42015, .T. ) ;
#24309=DIRECTION ( 'NONE',  ( -3.773278334444167608E-23, 1.000000000000000000, 0.000000000000000000 ) ) ;
#24310=CARTESIAN_POINT ( 'NONE',  ( -84.52287095715007581, -24.66019654487199730, 8.947790411086122830 ) ) ;
#24311=LINE ( 'NONE', #46158, #1960 ) ;
#24312=PLANE ( 'NONE',  #17086 ) ;
#24313=CARTESIAN_POINT ( 'NONE',  ( 11.77038589110637901, 16.27938679534767275, 11.49999999999998934 ) ) ;
#24314=CARTESIAN_POINT ( 'NONE',  ( -109.5571235402458967, -23.73766607897670156, -1.055555164236452903 ) ) ;
#24316=CARTESIAN_POINT ( 'NONE',  ( -66.53646650503104354, -24.66019654487199375, 8.947790411086119278 ) ) ;
#24317=CARTESIAN_POINT ( 'NONE',  ( 21.13568926591755925, -8.834425160694816981, 11.49999999999999645 ) ) ;
#24318=CARTESIAN_POINT ( 'NONE',  ( 20.46598465274837864, -9.837531852206524263, 11.49999999999998934 ) ) ;
#24319=ORIENTED_EDGE ( 'NONE', *, *, #62975, .T. ) ;
#24320=CARTESIAN_POINT ( 'NONE',  ( -30.47287095715007865, -24.66779572958783717, 8.870747851402812856 ) ) ;
#24321=LINE ( 'NONE', #87730, #41543 ) ;
#24322=CARTESIAN_POINT ( 'NONE',  ( -40.20933087355918900, -25.19828085996519818, 3.317003188998405960 ) ) ;
#24323=CARTESIAN_POINT ( 'NONE',  ( -100.6228709571500559, -29.50250786944525672, 11.44777988621623166 ) ) ;
#24325=CARTESIAN_POINT ( 'NONE',  ( -128.5903321797774765, -23.48786465467241769, 11.44779295918253403 ) ) ;
#24328=CARTESIAN_POINT ( 'NONE',  ( -98.95846461277810135, -25.25460634227597012, 5.689168979074962884 ) ) ;
#24332=CARTESIAN_POINT ( 'NONE',  ( -9.549598871097368047, 18.00506641634745009, -1.500000000000002220 ) ) ;
#24333=VERTEX_POINT ( 'NONE', #52070 ) ;
#24334=EDGE_CURVE ( 'NONE', #29240, #13848, #5883, .T. ) ;
#24335=CARTESIAN_POINT ( 'NONE',  ( -0.3492834940180428727, 22.98956000712751546, -1.500000000000002220 ) ) ;
#24336=CARTESIAN_POINT ( 'NONE',  ( -63.62287095715004881, -24.64898659630528499, 1.056161002820822592 ) ) ;
#24338=EDGE_LOOP ( 'NONE', ( #50105, #26544, #36084, #95457 ) ) ;
#24339=CARTESIAN_POINT ( 'NONE',  ( -114.5228709571501327, -23.96177878511310055, 10.65340807706329507 ) ) ;
#24340=EDGE_CURVE ( 'NONE', #30931, #65310, #59052, .T. ) ;
#24341=EDGE_CURVE ( 'NONE', #95739, #66931, #91611, .T. ) ;
#24343=CARTESIAN_POINT ( 'NONE',  ( -116.5120864331906319, -25.30063104534080054, 5.394122295771973441 ) ) ;
#24344=CARTESIAN_POINT ( 'NONE',  ( 18.63368790978032763, -10.32677859091227113, 11.49999999999999645 ) ) ;
#24345=ORIENTED_EDGE ( 'NONE', *, *, #57367, .T. ) ;
#24346=AXIS2_PLACEMENT_3D ( 'NONE', #99191, #37316, #60662 ) ;
#24347=ORIENTED_EDGE ( 'NONE', *, *, #83499, .F. ) ;
#24348=CARTESIAN_POINT ( 'NONE',  ( -13.35739915041183323, 17.77566839534079435, 11.49999999999998934 ) ) ;
#24349=CARTESIAN_POINT ( 'NONE',  ( -10.67548511050313209, -17.69376651829569269, -1.500000000000002220 ) ) ;
#24352=PLANE ( 'NONE',  #26846 ) ;
#24353=CARTESIAN_POINT ( 'NONE',  ( -95.50513609013532346, -24.73531770709095312, 8.716586749053508498 ) ) ;
#24355=FACE_OUTER_BOUND ( 'NONE', #28949, .T. ) ;
#24356=VERTEX_POINT ( 'NONE', #55570 ) ;
#24358=CARTESIAN_POINT ( 'NONE',  ( -70.80215084669140424, -25.14053967007993506, 6.999363323083984234 ) ) ;
#24359=CARTESIAN_POINT ( 'NONE',  ( -9.832896139050584239, -18.40278743011522877, -1.500000000000002220 ) ) ;
#24361=CARTESIAN_POINT ( 'NONE',  ( -21.80608713477256089, -0.9339522974687717305, 11.49999999999999645 ) ) ;
#24362=CARTESIAN_POINT ( 'NONE',  ( -102.6228709571501128, -23.96177878511309345, 10.65340807706329507 ) ) ;
#24363=CARTESIAN_POINT ( 'NONE',  ( -78.51252607565909614, -23.96169478059713498, 10.65365249895717881 ) ) ;
#24364=CARTESIAN_POINT ( 'NONE',  ( -14.31525571501011207, 17.33968770572689166, 11.49999999999998934 ) ) ;
#24366=CARTESIAN_POINT ( 'NONE',  ( -57.62287095715004881, -23.72747288104441665, -1.053458166803662666 ) ) ;
#24368=EDGE_CURVE ( 'NONE', #79014, #90831, #32449, .T. ) ;
#24369=ORIENTED_EDGE ( 'NONE', *, *, #45458, .T. ) ;
#24370=ORIENTED_EDGE ( 'NONE', *, *, #42916, .F. ) ;
#24371=EDGE_LOOP ( 'NONE', ( #69630, #84045, #32662, #23108 ) ) ;
#24372=ORIENTED_EDGE ( 'NONE', *, *, #4649, .F. ) ;
#24373=CARTESIAN_POINT ( 'NONE',  ( -6.079122355442096115, 20.50309271558274915, -1.500000000000002220 ) ) ;
#24374=CARTESIAN_POINT ( 'NONE',  ( 18.00092565640838416, -13.26076702590692769, 11.49999999999999645 ) ) ;
#24375=VERTEX_POINT ( 'NONE', #70785 ) ;
#24376=CARTESIAN_POINT ( 'NONE',  ( 18.71565868802652588, -9.641079743366450572, -1.500000000000002220 ) ) ;
#24377=DIRECTION ( 'NONE',  ( -3.773278334453079030E-23, 0.9999999999976377785, 2.173523156925979128E-06 ) ) ;
#24378=CARTESIAN_POINT ( 'NONE',  ( -15.85412420263326538, -12.13584807887712458, -1.500000000000002220 ) ) ;
#24381=CARTESIAN_POINT ( 'NONE',  ( 16.16784302627978320, -14.93143893958281154, -1.500000000000002220 ) ) ;
#24382=CARTESIAN_POINT ( 'NONE',  ( -83.52287095715009002, -24.50216790748204687, 0.6166512839542566127 ) ) ;
#24383=VERTEX_POINT ( 'NONE', #33215 ) ;
#24384=CARTESIAN_POINT ( 'NONE',  ( -38.62287095715005592, -23.47593901973091235, -1.443836447539011525 ) ) ;
#24385=LINE ( 'NONE', #8670, #66033 ) ;
#24386=CARTESIAN_POINT ( 'NONE',  ( -8.730572200882948053, 18.91488879456464289, 11.49999999999999645 ) ) ;
#24390=CARTESIAN_POINT ( 'NONE',  ( -48.55620429048340014, -23.47593901973091235, -1.443836447539009749 ) ) ;
#24391=CARTESIAN_POINT ( 'NONE',  ( -8.160016139516647726, -19.69179572373923648, -1.500000000000002220 ) ) ;
#24392=PLANE ( 'NONE',  #77437 ) ;
#24393=CARTESIAN_POINT ( 'NONE',  ( -51.29572423414915505, -25.26926909690447332, 3.940521613042322624 ) ) ;
#24394=AXIS2_PLACEMENT_3D ( 'NONE', #13995, #73916, #29232 ) ;
#24395=EDGE_CURVE ( 'NONE', #39871, #29452, #32252, .T. ) ;
#24396=LINE ( 'NONE', #18292, #38980 ) ;
#24398=CARTESIAN_POINT ( 'NONE',  ( 8.566404662457630437, 20.85315857434707709, -1.500000000000002220 ) ) ;
#24399=CARTESIAN_POINT ( 'NONE',  ( -83.58953762381673869, -24.66019654487199730, 8.947790411086112172 ) ) ;
#24400=ORIENTED_EDGE ( 'NONE', *, *, #85655, .T. ) ;
#24401=CARTESIAN_POINT ( 'NONE',  ( -79.20788237378963004, -25.30563682090317812, 5.076185341878163726 ) ) ;
#24403=CARTESIAN_POINT ( 'NONE',  ( -6.620539020842763911, -18.51205181221761720, 11.49999999999999645 ) ) ;
#24406=CARTESIAN_POINT ( 'NONE',  ( -119.5228709571500616, -24.50321055353805377, 9.387540953477511607 ) ) ;
#24407=ORIENTED_EDGE ( 'NONE', *, *, #73876, .T. ) ;
#24408=CARTESIAN_POINT ( 'NONE',  ( -99.58504710487255807, -24.65952944569304961, 1.056160979905703901 ) ) ;
#24409=CARTESIAN_POINT ( 'NONE',  ( -55.62287095715004170, -24.62226745350437440, 0.9660975649728266168 ) ) ;
#24410=DIRECTION ( 'NONE',  ( -4.522247983293619802E-39, -2.173523156893721996E-06, 0.9999999999976377785 ) ) ;
#24412=CARTESIAN_POINT ( 'NONE',  ( 19.48663422773152121, -3.193742178437300794, 11.49999999999998934 ) ) ;
#24413=AXIS2_PLACEMENT_3D ( 'NONE', #21883, #46751, #31013 ) ;
#24416=CARTESIAN_POINT ( 'NONE',  ( 2.165584020960389822, 20.11889322763239107, 11.49999999999999645 ) ) ;
#24420=EDGE_LOOP ( 'NONE', ( #52975, #46433, #74036, #17156 ) ) ;
#24426=CARTESIAN_POINT ( 'NONE',  ( -61.52287095715004028, -23.73907113216989018, -1.053371485793255014 ) ) ;
#24427=CARTESIAN_POINT ( 'NONE',  ( -19.32702923155483177, -5.217993511516596961, 11.49999999999998934 ) ) ;
#24428=CARTESIAN_POINT ( 'NONE',  ( -34.62287095715005592, -24.64898659630367206, 1.056161002820817485 ) ) ;
#24430=EDGE_LOOP ( 'NONE', ( #13280, #61689, #37333, #23983 ) ) ;
#24432=CARTESIAN_POINT ( 'NONE',  ( -110.1380102904055178, -25.29012728827590450, 3.309553723195009400 ) ) ;
#24433=CARTESIAN_POINT ( 'NONE',  ( -58.52287095715006160, -23.48786465467241058, 11.44779295918254824 ) ) ;
#24434=CARTESIAN_POINT ( 'NONE',  ( -106.5228709571500758, -23.48786465467242479, 11.44779295918253936 ) ) ;
#24435=CARTESIAN_POINT ( 'NONE',  ( -117.2170317540820861, -25.33540041250693875, 3.690481496468084988 ) ) ;
#24436=CARTESIAN_POINT ( 'NONE',  ( -83.55442932252776700, -23.96119346886880663, -0.6495511937832110227 ) ) ;
#24438=EDGE_CURVE ( 'NONE', #37312, #30827, #46816, .T. ) ;
#24439=CARTESIAN_POINT ( 'NONE',  ( -99.90616583242666593, -25.25978491487772004, 3.590542621692357717 ) ) ;
#24440=ORIENTED_EDGE ( 'NONE', *, *, #23048, .T. ) ;
#24442=CARTESIAN_POINT ( 'NONE',  ( 19.34776771173714849, 6.126202725962671458, -1.500000000000002220 ) ) ;
#24443=B_SPLINE_CURVE_WITH_KNOTS ( 'NONE', 3,
 ( #41864, #19501, #66711, #73790 ),
 .UNSPECIFIED., .F., .F.,
 ( 4, 4 ),
 ( 0.6502502522661839368, 0.6592566835382995816 ),
 .UNSPECIFIED. ) ;
#24445=EDGE_CURVE ( 'NONE', #59566, #88484, #10377, .T. ) ;
#24446=B_SPLINE_CURVE_WITH_KNOTS ( 'NONE', 3,
 ( #68238, #92061, #37286, #93547 ),
 .UNSPECIFIED., .F., .F.,
 ( 4, 4 ),
 ( 0.3800573141027208113, 0.3890637453748362340 ),
 .UNSPECIFIED. ) ;
#24447=CARTESIAN_POINT ( 'NONE',  ( -59.52207684527606801, -23.48786465467241058, 11.44779295918255357 ) ) ;
#24448=EDGE_CURVE ( 'NONE', #96886, #99590, #37105, .T. ) ;
#24449=ORIENTED_EDGE ( 'NONE', *, *, #26241, .T. ) ;
#24450=CARTESIAN_POINT ( 'NONE',  ( -94.58953762381672448, -23.47596703998600631, 11.44779298504227683 ) ) ;
#24451=CARTESIAN_POINT ( 'NONE',  ( -15.75104486599040321, 12.61009050114280861, -1.500000000000002220 ) ) ;
#24452=EDGE_CURVE ( 'NONE', #92846, #6893, #79531, .T. ) ;
#24453=CARTESIAN_POINT ( 'NONE',  ( -4.502559807402421121, -20.62786074129878955, 11.49999999999999645 ) ) ;
#24454=CARTESIAN_POINT ( 'NONE',  ( -19.88706384024380824, 9.709922325909349894, 11.49999999999998934 ) ) ;
#24455=EDGE_CURVE ( 'NONE', #34094, #5846, #19067, .T. ) ;
#24456=VECTOR ( 'NONE', #69714, 1000.000000000000114 ) ;
#24457=CARTESIAN_POINT ( 'NONE',  ( -19.39287000742378453, 6.875061630626206011, 11.49999999999998934 ) ) ;
#24458=CARTESIAN_POINT ( 'NONE',  ( -55.52287095715008292, -24.82558206586143612, 1.605769216559449486 ) ) ;
#24462=PLANE ( 'NONE',  #65694 ) ;
#24467=CARTESIAN_POINT ( 'NONE',  ( -100.5228709571500616, -24.99132157543084531, 2.256160258750667502 ) ) ;
#24470=CARTESIAN_POINT ( 'NONE',  ( -20.69558417703438025, 1.077208295497980250, -1.500000000000002220 ) ) ;
#24471=CARTESIAN_POINT ( 'NONE',  ( 21.21565077533257337, 4.556159429511043690, 11.49999999999999645 ) ) ;
#24472=ORIENTED_EDGE ( 'NONE', *, *, #8182, .F. ) ;
#24473=CARTESIAN_POINT ( 'NONE',  ( -106.6228709571500559, -29.50248528299804818, 1.056150453629043584 ) ) ;
#24475=CARTESIAN_POINT ( 'NONE',  ( 5.437191932089902480, -21.69250089042843754, 11.49999999999998934 ) ) ;
#24476=CARTESIAN_POINT ( 'NONE',  ( -47.52204401451512439, -23.48786465467240347, 11.44779295918255002 ) ) ;
#24477=PLANE ( 'NONE',  #54574 ) ;
#24478=ORIENTED_EDGE ( 'NONE', *, *, #27290, .F. ) ;
#24481=CARTESIAN_POINT ( 'NONE',  ( -35.47580382915101183, -24.73531770709095312, 8.716586749053508498 ) ) ;
#24483=ORIENTED_EDGE ( 'NONE', *, *, #39914, .F. ) ;
#24487=CARTESIAN_POINT ( 'NONE',  ( -4.955175619359221351, 20.59750927568439138, -1.500000000000002220 ) ) ;
#24489=CARTESIAN_POINT ( 'NONE',  ( -50.57648070875571733, -24.92564183028979130, 1.928384488918255535 ) ) ;
#24490=CARTESIAN_POINT ( 'NONE',  ( 1.801620404824296084, -21.73869551012647605, -1.500000000000002220 ) ) ;
#24491=DIRECTION ( 'NONE',  ( 0.000000000000000000, -0.9999999999976377785, -2.173523156925979975E-06 ) ) ;
#24492=DIRECTION ( 'NONE',  ( -3.773278334453079618E-23, 0.9999999999976377785, 2.173523156925979975E-06 ) ) ;
#24494=CARTESIAN_POINT ( 'NONE',  ( -21.44618410820073606, 4.064364382921047181, -1.500000000000002220 ) ) ;
#24495=CARTESIAN_POINT ( 'NONE',  ( -30.57287095715006586, -24.48248896992290469, 0.5825846392791583783 ) ) ;
#24496=VERTEX_POINT ( 'NONE', #19483 ) ;
#24501=CARTESIAN_POINT ( 'NONE',  ( -129.5219154021366137, -24.35071581493544102, 9.817618358456021710 ) ) ;
#24503=VERTEX_POINT ( 'NONE', #42358 ) ;
#24504=CARTESIAN_POINT ( 'NONE',  ( -29.24636659180999843, -25.20264517434234364, 4.940287045316306802 ) ) ;
#24505=CARTESIAN_POINT ( 'NONE',  ( -82.58825244796760501, -24.34968618360933945, 0.1864209137778926328 ) ) ;
#24506=CARTESIAN_POINT ( 'NONE',  ( 17.84191302092929021, 11.53353326677314961, 11.49999999999998934 ) ) ;
#24507=CARTESIAN_POINT ( 'NONE',  ( -94.60069243175672682, -23.48783264082477373, -1.443836473390087249 ) ) ;
#24508=CARTESIAN_POINT ( 'NONE',  ( -41.52287095715006870, -24.65952944569304606, 1.056160979905691910 ) ) ;
#24510=CARTESIAN_POINT ( 'NONE',  ( -61.62287095715004881, -29.50248528299804818, 1.056150453629034924 ) ) ;
#24511=CARTESIAN_POINT ( 'NONE',  ( -127.5228709571500332, -24.66019654487200441, 8.947790411086105067 ) ) ;
#24512=CARTESIAN_POINT ( 'NONE',  ( 8.665315094346039970, 17.34094453737590769, -1.500000000000002220 ) ) ;
#24514=CARTESIAN_POINT ( 'NONE',  ( -117.6250629353716590, -24.35071581493544457, 9.817618358456019934 ) ) ;
#24515=ORIENTED_EDGE ( 'NONE', *, *, #36053, .F. ) ;
#24516=CARTESIAN_POINT ( 'NONE',  ( -9.627943313441900131, 16.98966435471970726, 11.49999999999999645 ) ) ;
#24518=CARTESIAN_POINT ( 'NONE',  ( -79.45589157972931105, -25.21686183209924792, 6.470215754339476710 ) ) ;
#24519=VERTEX_POINT ( 'NONE', #51447 ) ;
#24521=CARTESIAN_POINT ( 'NONE',  ( -89.59156628431851743, -24.15543982623907482, -0.2315651400026483009 ) ) ;
#24522=CARTESIAN_POINT ( 'NONE',  ( -30.47287095715007510, -23.47593906522708451, -1.422904450652597852 ) ) ;
#24523=CARTESIAN_POINT ( 'NONE',  ( -55.62287095715006302, -24.63287334234180292, 0.9662140553045335256 ) ) ;
#24524=CARTESIAN_POINT ( 'NONE',  ( -11.90832679833862073, -15.64659449181510986, -1.500000000000002220 ) ) ;
#24526=CARTESIAN_POINT ( 'NONE',  ( 21.32721141102669193, -3.434809268862642817, 11.49999999999998934 ) ) ;
#24527=B_SPLINE_CURVE_WITH_KNOTS ( 'NONE', 3,
 ( #68155, #69654, #29580, #7235, #60557, #100064 ),
 .UNSPECIFIED., .F., .F.,
 ( 4, 2, 4 ),
 ( 0.000000000000000000, 0.001380764517853254455, 0.002761529035706508910 ),
 .UNSPECIFIED. ) ;
#24528=CARTESIAN_POINT ( 'NONE',  ( -85.55620429048337883, -25.00182538069145721, 7.747789668545100206 ) ) ;
#24530=CARTESIAN_POINT ( 'NONE',  ( -50.62287095715005592, -29.50248528299804818, 1.056150453629033370 ) ) ;
#24531=CARTESIAN_POINT ( 'NONE',  ( 6.977686149863070675, -22.03694335537135984, -1.500000000000002220 ) ) ;
#24536=CARTESIAN_POINT ( 'NONE',  ( -121.5228709571500616, -29.50248528299804818, 1.056150453629045360 ) ) ;
#24538=CARTESIAN_POINT ( 'NONE',  ( -101.9131232614075770, -25.23352619098501393, 6.415922869675740436 ) ) ;
#24539=CARTESIAN_POINT ( 'NONE',  ( -110.7466941838547143, -25.29823823612047917, 2.889690974355013875 ) ) ;
#24540=CARTESIAN_POINT ( 'NONE',  ( -110.6228709571500701, -23.48786465467241769, 11.44779295918254114 ) ) ;
#24541=CARTESIAN_POINT ( 'NONE',  ( -99.41873814713473223, -25.31566058944073916, 4.744921480468723196 ) ) ;
#24542=CARTESIAN_POINT ( 'NONE',  ( 5.901097582950029619, 19.04237314665466485, 11.49999999999998934 ) ) ;
#24543=CARTESIAN_POINT ( 'NONE',  ( -75.50775092909401565, -24.15602025860895807, 10.28564288303536678 ) ) ;
#24544=CARTESIAN_POINT ( 'NONE',  ( 8.478510716907816658, 17.93336729499101523, -1.500000000000002220 ) ) ;
#24545=VERTEX_POINT ( 'NONE', #95618 ) ;
#24547=VECTOR ( 'NONE', #61383, 1000.000000000000114 ) ;
#24549=CARTESIAN_POINT ( 'NONE',  ( -39.44256650533377950, -25.29116604522729972, 3.228027748310828837 ) ) ;
#24551=CARTESIAN_POINT ( 'NONE',  ( 3.485566553294195291, 20.44204155273375889, 11.49999999999999645 ) ) ;
#24552=DIRECTION ( 'NONE',  ( -3.773278334453079618E-23, 0.9999999999976377785, 2.173523156925979975E-06 ) ) ;
#24553=CARTESIAN_POINT ( 'NONE',  ( -106.5889902452000939, -24.34968618360933945, 0.1864209137778878034 ) ) ;
#24554=CARTESIAN_POINT ( 'NONE',  ( 15.23092229589061830, -16.91372389758942418, 11.49999999999999645 ) ) ;
#24556=CARTESIAN_POINT ( 'NONE',  ( -69.60831051794583857, -23.48783264082476308, -1.443836473390097908 ) ) ;
#24557=CARTESIAN_POINT ( 'NONE',  ( -90.62287095715004170, -23.47596703998600631, 11.44779298504227860 ) ) ;
#24559=CARTESIAN_POINT ( 'NONE',  ( 2.532258636284850706, -20.04889675553949147, -1.500000000000002220 ) ) ;
#24560=CARTESIAN_POINT ( 'NONE',  ( -43.62287095715004170, -23.48786465467241058, 11.44779295918255180 ) ) ;
#24563=CARTESIAN_POINT ( 'NONE',  ( -70.62287095715001328, -24.51254535404256529, 9.355368623467642308 ) ) ;
#24564=CARTESIAN_POINT ( 'NONE',  ( -14.98413761715186077, 17.36544542080599740, 11.49999999999998934 ) ) ;
#24566=CARTESIAN_POINT ( 'NONE',  ( -17.62595516807937557, -9.487554784798948759, -1.500000000000002220 ) ) ;
#24569=CARTESIAN_POINT ( 'NONE',  ( -3.838044578953509145, 20.63102806057878880, 11.49999999999999645 ) ) ;
#24570=CARTESIAN_POINT ( 'NONE',  ( -48.52287095715004739, -23.48783264083430211, -1.443836473375264440 ) ) ;
#24571=CARTESIAN_POINT ( 'NONE',  ( -69.08877929746488178, -25.31612571981231596, 5.548814315813750397 ) ) ;
#24572=CARTESIAN_POINT ( 'NONE',  ( -14.94409825380703616, 16.19114737329946507, -1.500000000000002220 ) ) ;
#24573=EDGE_CURVE ( 'NONE', #62281, #90808, #4275, .T. ) ;
#24575=ORIENTED_EDGE ( 'NONE', *, *, #16893, .F. ) ;
#24576=VECTOR ( 'NONE', #55597, 1000.000000000000114 ) ;
#24577=CARTESIAN_POINT ( 'NONE',  ( -118.5228709571501184, -24.66019654487200441, 8.947790411086110396 ) ) ;
#24579=ORIENTED_EDGE ( 'NONE', *, *, #28242, .F. ) ;
#24583=ORIENTED_EDGE ( 'NONE', *, *, #7905, .F. ) ;
#24588=CARTESIAN_POINT ( 'NONE',  ( 10.78675619948152864, -17.38023510967517637, -1.500000000000002220 ) ) ;
#24589=ORIENTED_EDGE ( 'NONE', *, *, #58901, .F. ) ;
#24590=CARTESIAN_POINT ( 'NONE',  ( -106.5228709571500758, -24.66019654487200441, 8.947790411086112172 ) ) ;
#24591=CARTESIAN_POINT ( 'NONE',  ( -44.53465503250131263, -24.51314013834316086, 0.6176544820404110681 ) ) ;
#24592=CARTESIAN_POINT ( 'NONE',  ( -77.55620429048339304, -24.64898659630529210, 1.056161002820828809 ) ) ;
#24593=CARTESIAN_POINT ( 'NONE',  ( -21.75032768068154354, -4.810781854073628239, -1.500000000000002220 ) ) ;
#24594=CARTESIAN_POINT ( 'NONE',  ( -70.44736088819470865, -25.13396146398487119, 7.096960098442634646 ) ) ;
#24595=CARTESIAN_POINT ( 'NONE',  ( -90.55620429048337883, -24.99156044556202971, 7.747789690856174083 ) ) ;
#24596=ORIENTED_EDGE ( 'NONE', *, *, #5546, .F. ) ;
#24597=CARTESIAN_POINT ( 'NONE',  ( -96.62287095715004170, -24.65952944569304606, 1.056160979905703456 ) ) ;
#24598=CARTESIAN_POINT ( 'NONE',  ( -118.5228709571500758, -23.47593901973090524, -1.443836447538996204 ) ) ;
#24599=CARTESIAN_POINT ( 'NONE',  ( -12.40256906124370673, -16.71776976679197801, 11.49999999999998934 ) ) ;
#24602=ORIENTED_EDGE ( 'NONE', *, *, #53688, .T. ) ;
#24604=CARTESIAN_POINT ( 'NONE',  ( -50.40445135320379677, -25.25854569424054219, 7.101635264402184511 ) ) ;
#24605=CARTESIAN_POINT ( 'NONE',  ( -17.93810645791062441, 10.97360191750010827, -1.500000000000002220 ) ) ;
#24610=CARTESIAN_POINT ( 'NONE',  ( -101.6175123368144142, -25.25419440104175095, 7.038108131071323825 ) ) ;
#24611=CARTESIAN_POINT ( 'NONE',  ( -110.2244512850201659, -25.12087729867975483, 2.834499938438063360 ) ) ;
#24612=CARTESIAN_POINT ( 'NONE',  ( -63.62287095715004881, -24.64898659630528499, 1.056161002820822592 ) ) ;
#24613=CARTESIAN_POINT ( 'NONE',  ( 5.796264663052079769, -21.44337444023769379, 11.49999999999999645 ) ) ;
#24614=ORIENTED_EDGE ( 'NONE', *, *, #82579, .F. ) ;
#24616=CARTESIAN_POINT ( 'NONE',  ( -71.18699820573013426, -25.28351461562841607, 5.743153344412908368 ) ) ;
#24617=EDGE_LOOP ( 'NONE', ( #77514, #22809, #56941, #37368 ) ) ;
#24618=CARTESIAN_POINT ( 'NONE',  ( -18.33335541821337245, -13.34141728429830742, 11.49999999999998934 ) ) ;
#24620=EDGE_LOOP ( 'NONE', ( #83882, #43566, #93216, #37564 ) ) ;
#24622=VECTOR ( 'NONE', #21142, 1000.000000000000114 ) ;
#24626=EDGE_CURVE ( 'NONE', #1265, #60838, #18951, .T. ) ;
#24627=CARTESIAN_POINT ( 'NONE',  ( -3.510519812331947875, -19.85243952969433323, 11.49999999999998934 ) ) ;
#24630=DIRECTION ( 'NONE',  ( -3.773278334453079618E-23, 0.9999999999976377785, 2.173523156925979975E-06 ) ) ;
#24631=CARTESIAN_POINT ( 'NONE',  ( -22.40390758644239710, -1.035154934579901820, -1.500000000000002220 ) ) ;
#24632=B_SPLINE_CURVE_WITH_KNOTS ( 'NONE', 3,
 ( #11335, #42311, #26056, #50404, #57028, #73729 ),
 .UNSPECIFIED., .F., .F.,
 ( 4, 2, 4 ),
 ( 6.396480873082856813E-06, 0.001387752211907360709, 0.002769107942941638652 ),
 .UNSPECIFIED. ) ;
#24633=ORIENTED_EDGE ( 'NONE', *, *, #24050, .F. ) ;
#24634=VERTEX_POINT ( 'NONE', #20477 ) ;
#24640=CARTESIAN_POINT ( 'NONE',  ( -13.18904525526904692, 14.46673508071025971, 11.49999999999998934 ) ) ;
#24643=CARTESIAN_POINT ( 'NONE',  ( 7.367719877546908158, -20.20905560389912026, -1.500000000000002220 ) ) ;
#24644=LINE ( 'NONE', #39881, #98164 ) ;
#24648=CARTESIAN_POINT ( 'NONE',  ( 19.50756536182865020, -12.10693203178887423, -1.500000000000002220 ) ) ;
#24650=VECTOR ( 'NONE', #100235, 1000.000000000000114 ) ;
#24652=CARTESIAN_POINT ( 'NONE',  ( -93.62287095715007013, -23.96127896941632685, -0.6493128931037834839 ) ) ;
#24653=CARTESIAN_POINT ( 'NONE',  ( -53.52206055214148250, -23.48783264082476663, -1.443836473390096353 ) ) ;
#24654=CARTESIAN_POINT ( 'NONE',  ( 16.02535498940104830, 12.03463022438520191, 11.49999999999999645 ) ) ;
#24656=DIRECTION ( 'NONE',  ( -3.773278334453079618E-23, 0.9999999999976377785, 2.173523156925979975E-06 ) ) ;
#24658=CARTESIAN_POINT ( 'NONE',  ( -39.55620429048340014, -23.47596703998600276, 11.44779298504227505 ) ) ;
#24659=CARTESIAN_POINT ( 'NONE',  ( -65.52287095715006160, -23.47593901973090169, -1.443836447538996870 ) ) ;
#24660=CARTESIAN_POINT ( 'NONE',  ( 21.64095104908334122, -2.195182070091274529, 11.49999999999998934 ) ) ;
#24661=EDGE_CURVE ( 'NONE', #21356, #47882, #28668, .T. ) ;
#24662=CARTESIAN_POINT ( 'NONE',  ( -90.62287095715004170, -23.48786465467241058, 11.44779295918254469 ) ) ;
#24663=CARTESIAN_POINT ( 'NONE',  ( 14.10018531369908423, 13.67006465538575277, -1.500000000000002220 ) ) ;
#24664=CARTESIAN_POINT ( 'NONE',  ( -122.6228709571500701, -24.34917612406838572, 0.1852690917426738082 ) ) ;
#24665=CARTESIAN_POINT ( 'NONE',  ( -40.94614453995487935, -25.19886899424074400, 3.394663469267442224 ) ) ;
#24667=AXIS2_PLACEMENT_3D ( 'NONE', #23147, #23655, #47015 ) ;
#24670=CARTESIAN_POINT ( 'NONE',  ( -11.90445915685808131, 16.78794160864392992, 11.49999999999999645 ) ) ;
#24671=CARTESIAN_POINT ( 'NONE',  ( -118.5228709571500758, -29.50248528299804818, 1.056150453629045360 ) ) ;
#24672=AXIS2_PLACEMENT_3D ( 'NONE', #3490, #34429, #96325 ) ;
#24673=CARTESIAN_POINT ( 'NONE',  ( -120.5173596569751311, -24.73486907724918638, 1.287355809206965684 ) ) ;
#24674=CARTESIAN_POINT ( 'NONE',  ( 11.79716412695777272, 19.27136520130675024, 11.49999999999999645 ) ) ;
#24675=ORIENTED_EDGE ( 'NONE', *, *, #76772, .T. ) ;
#24676=CARTESIAN_POINT ( 'NONE',  ( -99.52927036222322954, -25.26387300713328443, 4.031758623024652266 ) ) ;
#24677=CARTESIAN_POINT ( 'NONE',  ( -37.52287095715008292, -23.72747288104470087, -1.053458166803228124 ) ) ;
#24678=CARTESIAN_POINT ( 'NONE',  ( -125.5192790873664279, -25.00182538069147498, 7.747789668545045139 ) ) ;
#24680=EDGE_CURVE ( 'NONE', #44828, #83541, #2093, .T. ) ;
#24681=CARTESIAN_POINT ( 'NONE',  ( -26.14934357328621317, -24.93063460670250109, 7.450064799070047705 ) ) ;
#24682=CARTESIAN_POINT ( 'NONE',  ( -28.52287095715005805, -24.49960542107631056, 8.947790409070465856 ) ) ;
#24685=CARTESIAN_POINT ( 'NONE',  ( -79.34687923781920915, -25.31596438058133813, 5.960409178060182889 ) ) ;
#24686=CARTESIAN_POINT ( 'NONE',  ( -21.14637036216210575, 8.611126525438130841, 11.49999999999998934 ) ) ;
#24688=CARTESIAN_POINT ( 'NONE',  ( -72.52287095715010423, -24.66019654487199375, 8.947790411086128159 ) ) ;
#24689=CARTESIAN_POINT ( 'NONE',  ( -63.60363133230624300, -23.73791477778912196, 11.05961554403170766 ) ) ;
#24691=EDGE_CURVE ( 'NONE', #923, #39432, #99582, .T. ) ;
#24692=CARTESIAN_POINT ( 'NONE',  ( -11.43049785330379997, -19.34545768653811493, 11.49999999999999645 ) ) ;
#24693=ORIENTED_EDGE ( 'NONE', *, *, #25982, .T. ) ;
#24694=CARTESIAN_POINT ( 'NONE',  ( -70.62287095715004170, -23.48786465467241058, 11.44779295918254469 ) ) ;
#24695=CARTESIAN_POINT ( 'NONE',  ( -12.46176837856299002, 18.05058065364367792, 11.49999999999998934 ) ) ;
#24696=EDGE_CURVE ( 'NONE', #84956, #87003, #83220, .T. ) ;
#24697=LINE ( 'NONE', #64300, #78592 ) ;
#24698=CARTESIAN_POINT ( 'NONE',  ( -110.5228709571500616, -25.00158670708909625, 2.256160236439166411 ) ) ;
#24700=AXIS2_PLACEMENT_3D ( 'NONE', #70338, #54616, #78433 ) ;
#24702=CARTESIAN_POINT ( 'NONE',  ( -48.62369553988378357, -24.66019654487199730, 8.947790411086119278 ) ) ;
#24703=PLANE ( 'NONE',  #68924 ) ;
#24704=EDGE_LOOP ( 'NONE', ( #57802, #47931, #58589, #54968 ) ) ;
#24705=CARTESIAN_POINT ( 'NONE',  ( -18.14515864413662172, 9.488524743509296755, 11.49999999999998934 ) ) ;
#24707=ORIENTED_EDGE ( 'NONE', *, *, #100027, .T. ) ;
#24708=AXIS2_PLACEMENT_3D ( 'NONE', #96616, #43842, #26620 ) ;
#24709=EDGE_LOOP ( 'NONE', ( #57431, #30984, #49446, #64475 ) ) ;
#24710=EDGE_LOOP ( 'NONE', ( #33322, #31959, #21969, #93915 ) ) ;
#24711=CARTESIAN_POINT ( 'NONE',  ( 6.910522817300494225, 22.03692736239173300, -1.500000000000002220 ) ) ;
#24712=DIRECTION ( 'NONE',  ( -1.000000000000000000, -3.773278334444166432E-23, -8.201307841325785021E-29 ) ) ;
#24713=ADVANCED_FACE ( 'NONE', ( #45823 ), #59564, .F. ) ;
#24714=CARTESIAN_POINT ( 'NONE',  ( -20.21730713243277933, 1.494317884549376974, -1.500000000000002220 ) ) ;
#24715=VERTEX_POINT ( 'NONE', #68664 ) ;
#24717=DIRECTION ( 'NONE',  ( -3.773278334453079030E-23, 0.9999999999976377785, 2.173523156925979128E-06 ) ) ;
#24720=CARTESIAN_POINT ( 'NONE',  ( -11.48222599368078889, -18.13851731312990267, 11.49999999999999645 ) ) ;
#24722=CARTESIAN_POINT ( 'NONE',  ( -75.59707762896087502, -24.15503026093913874, -0.2815557561904522554 ) ) ;
#24723=CARTESIAN_POINT ( 'NONE',  ( -48.58953762381672448, -24.64898659630528144, 1.056161002820820372 ) ) ;
#24724=EDGE_LOOP ( 'NONE', ( #23051, #10239, #17012, #71019 ) ) ;
#24725=CARTESIAN_POINT ( 'NONE',  ( -7.464567774302189207, 19.34240081622845153, 11.49999999999998934 ) ) ;
#24726=VERTEX_POINT ( 'NONE', #13863 ) ;
#24727=CARTESIAN_POINT ( 'NONE',  ( -125.5916854314852458, -23.48783264082478794, -1.443836473390061936 ) ) ;
#24728=VERTEX_POINT ( 'NONE', #90497 ) ;
#24730=B_SPLINE_SURFACE_WITH_KNOTS ( 'NONE', 3, 3, ( 
 ( #48390, #96062, #2723, #88949 ),
 ( #25546, #47891, #87443, #41792 ),
 ( #56012, #86939, #10320, #57015 ),
 ( #17430, #40273, #78809, #63630 ),
 ( #3235, #95559, #41275, #72229 ),
 ( #64643, #26041, #73231, #1716 ),
 ( #79325, #65636, #3723, #9819 ) ),
 .UNSPECIFIED., .F., .F., .F.,
 ( 4, 3, 4 ),
 ( 4, 4 ),
 ( 0.7945040050992240310, 0.8970133687736500105, 0.9995227324480759901 ),
 ( 0.3295777475180419747, 0.3307426270317702643 ),
 .UNSPECIFIED. ) ;
#24732=B_SPLINE_CURVE_WITH_KNOTS ( 'NONE', 3,
 ( #91385, #53842, #69564, #21862, #60957, #54344, #23360, #13755, #42, #61457, #15261, #21367, #69053, #38100 ),
 .UNSPECIFIED., .F., .F.,
 ( 4, 2, 2, 2, 2, 2, 4 ),
 ( 0.000000000000000000, 0.0004063758915776106203, 0.0008127517831552199395, 0.001015939728944024491, 0.001219127674732828608, 0.001422315620521632726, 0.001625503566310437060 ),
 .UNSPECIFIED. ) ;
#24733=CARTESIAN_POINT ( 'NONE',  ( -117.5228709571500758, -24.65952944569305316, 1.056160979905705899 ) ) ;
#24734=ORIENTED_EDGE ( 'NONE', *, *, #31008, .T. ) ;
#24738=CARTESIAN_POINT ( 'NONE',  ( -66.52287095715003318, -24.66019654487199375, 8.947790411086119278 ) ) ;
#24739=CARTESIAN_POINT ( 'NONE',  ( -21.82725030464235516, 2.967780500094957308, 11.49999999999999645 ) ) ;
#24740=CARTESIAN_POINT ( 'NONE',  ( -43.52287095715006160, -29.50247984919015209, -1.443849546365060466 ) ) ;
#24741=CARTESIAN_POINT ( 'NONE',  ( -4.885077187424587741, 22.05487924249641551, 11.49999999999998934 ) ) ;
#24742=CARTESIAN_POINT ( 'NONE',  ( 19.96068868648078620, -6.529529906025321573, -1.500000000000002220 ) ) ;
#24743=CARTESIAN_POINT ( 'NONE',  ( -62.52287095715007581, -23.72747288104470087, -1.053458166803227458 ) ) ;
#24746=ORIENTED_EDGE ( 'NONE', *, *, #71363, .F. ) ;
#24747=CARTESIAN_POINT ( 'NONE',  ( -80.62287095715008434, -24.82558206586145033, 1.605769216559443491 ) ) ;
#24748=EDGE_CURVE ( 'NONE', #6143, #94577, #68558, .T. ) ;
#24750=ORIENTED_EDGE ( 'NONE', *, *, #88393, .T. ) ;
#24751=CARTESIAN_POINT ( 'NONE',  ( 1.363997202867437863, 21.09336101032836908, -1.500000000000002220 ) ) ;
#24753=CARTESIAN_POINT ( 'NONE',  ( -51.93023907722363219, -25.26040824531888518, 6.217084455637032825 ) ) ;
#24754=CARTESIAN_POINT ( 'NONE',  ( -121.5573556918825204, -23.48783264082477373, -1.443836473390087916 ) ) ;
#24755=CARTESIAN_POINT ( 'NONE',  ( -118.5895376238167245, -23.47593901973091235, -1.443836447538997536 ) ) ;
#24757=CARTESIAN_POINT ( 'NONE',  ( 10.53326394202159300, -19.55463526559320542, -1.500000000000002220 ) ) ;
#24761=CARTESIAN_POINT ( 'NONE',  ( -37.49782949886290595, -24.15543982623907127, -0.2315651400026566831 ) ) ;
#24762=CARTESIAN_POINT ( 'NONE',  ( -126.5549976813165642, -24.51314013834316086, 0.6176544820404181735 ) ) ;
#24763=CARTESIAN_POINT ( 'NONE',  ( -41.86995616089613748, -25.27977532709532227, 4.210709737483026238 ) ) ;
#24765=AXIS2_PLACEMENT_3D ( 'NONE', #90687, #29286, #52133 ) ;
#24766=CARTESIAN_POINT ( 'NONE',  ( 19.32586673001642197, -2.567307930040524599, 11.49999999999998934 ) ) ;
#24767=EDGE_LOOP ( 'NONE', ( #17863, #99022, #85165, #71693 ) ) ;
#24768=CARTESIAN_POINT ( 'NONE',  ( -9.924231251898440576, -18.97836718215353713, -1.500000000000002220 ) ) ;
#24769=DIRECTION ( 'NONE',  ( -3.773278334444166432E-23, 1.000000000000000000, 0.000000000000000000 ) ) ;
#24770=CARTESIAN_POINT ( 'NONE',  ( -60.64669611341108890, -24.15602025861359792, 10.28564288302606045 ) ) ;
#24771=CARTESIAN_POINT ( 'NONE',  ( -51.63318508066054591, -24.34968618360933590, 0.1864209137778788938 ) ) ;
#24772=CARTESIAN_POINT ( 'NONE',  ( -38.52287095715006870, -24.65952944569303895, 1.056160979905691910 ) ) ;
#24773=CARTESIAN_POINT ( 'NONE',  ( -22.70586268970451371, -1.818501321912391999, -1.500000000000002220 ) ) ;
#24775=VECTOR ( 'NONE', #61260, 1000.000000000000114 ) ;
#24777=LINE ( 'NONE', #953, #46011 ) ;
#24778=CARTESIAN_POINT ( 'NONE',  ( 6.283368587668265448, -18.83516890145298106, 11.49999999999999645 ) ) ;
#24779=CARTESIAN_POINT ( 'NONE',  ( -123.5918566822411009, -23.48786465467241769, 11.44779295918253759 ) ) ;
#24782=CARTESIAN_POINT ( 'NONE',  ( -89.81226385320384509, -25.12770589570459379, 7.104042815775061470 ) ) ;
#24784=ORIENTED_EDGE ( 'NONE', *, *, #1923, .T. ) ;
#24787=CARTESIAN_POINT ( 'NONE',  ( -51.43440959051734751, -25.10935856805285482, 3.290885709867275910 ) ) ;
#24788=CARTESIAN_POINT ( 'NONE',  ( -14.64807036877012258, -15.96857234361563904, -1.500000000000002220 ) ) ;
#24789=ADVANCED_FACE ( 'NONE', ( #45333 ), #51583, .T. ) ;
#24790=CARTESIAN_POINT ( 'NONE',  ( -29.62287095715005947, -24.26261939641257825, 9.819270444555529664 ) ) ;
#24791=CARTESIAN_POINT ( 'NONE',  ( -1.849579639615634097, -19.42000222497389927, -1.500000000000002220 ) ) ;
#24792=ADVANCED_FACE ( 'NONE', ( #55948 ), #2165, .T. ) ;
#24793=CARTESIAN_POINT ( 'NONE',  ( -55.52645046534955497, -25.00182538069146787, 7.747789668545041586 ) ) ;
#24794=ORIENTED_EDGE ( 'NONE', *, *, #59283, .T. ) ;
#24795=ADVANCED_FACE ( 'NONE', ( #40211 ), #66157, .T. ) ;
#24796=CARTESIAN_POINT ( 'NONE',  ( 13.37706023731332827, -15.40713922116925616, 11.49999999999999645 ) ) ;
#24798=PLANE ( 'NONE',  #14010 ) ;
#24799=ORIENTED_EDGE ( 'NONE', *, *, #69853, .F. ) ;
#24800=CARTESIAN_POINT ( 'NONE',  ( -30.63208233338744080, -23.87624887660337691, 11.01174216662000127 ) ) ;
#24802=CARTESIAN_POINT ( 'NONE',  ( -39.04454818115137016, -25.31628458813839444, 4.262458856014446518 ) ) ;
#24805=CARTESIAN_POINT ( 'NONE',  ( 4.282148337517553749, -19.64591042314588165, -1.500000000000002220 ) ) ;
#24806=EDGE_CURVE ( 'NONE', #46271, #22334, #60136, .T. ) ;
#24807=CARTESIAN_POINT ( 'NONE',  ( -57.58953762381672448, -23.47593901973091235, -1.443836447539007972 ) ) ;
#24809=ORIENTED_EDGE ( 'NONE', *, *, #54540, .F. ) ;
#24811=CARTESIAN_POINT ( 'NONE',  ( 15.56936346670522120, 16.85858822313069894, 11.49999999999999645 ) ) ;
#24812=CARTESIAN_POINT ( 'NONE',  ( 7.533951754900199305, 21.46025436219600024, -1.500000000000002220 ) ) ;
#24813=ORIENTED_EDGE ( 'NONE', *, *, #6075, .F. ) ;
#24814=CARTESIAN_POINT ( 'NONE',  ( -31.55620429048339304, -23.47596703998600276, 11.44779298504227505 ) ) ;
#24817=CARTESIAN_POINT ( 'NONE',  ( -90.59125879922106606, -24.40034930558990922, 0.3402023900116054045 ) ) ;
#24818=PLANE ( 'NONE',  #7625 ) ;
#24819=EDGE_CURVE ( 'NONE', #58107, #9739, #85371, .T. ) ;
#24820=B_SPLINE_CURVE_WITH_KNOTS ( 'NONE', 3,
 ( #40920, #95706, #18080, #72380, #25691, #49048 ),
 .UNSPECIFIED., .F., .F.,
 ( 4, 2, 4 ),
 ( 0.000000000000000000, 0.001380764517853247516, 0.002761529035706495033 ),
 .UNSPECIFIED. ) ;
#24822=EDGE_CURVE ( 'NONE', #80762, #15342, #27417, .T. ) ;
#24823=CARTESIAN_POINT ( 'NONE',  ( -115.6228709571500417, -24.63287334234178516, 0.9662140553045511782 ) ) ;
#24824=CARTESIAN_POINT ( 'NONE',  ( -54.52287095715009002, -24.33832256527048088, 0.1851278514138564868 ) ) ;
#24825=CARTESIAN_POINT ( 'NONE',  ( -81.52287095715010423, -23.47593901973090524, -1.443836447538996648 ) ) ;
#24826=ORIENTED_EDGE ( 'NONE', *, *, #12424, .F. ) ;
#24827=CARTESIAN_POINT ( 'NONE',  ( 13.37706023731332827, -15.40713922116925616, -1.500000000000002220 ) ) ;
#24828=VERTEX_POINT ( 'NONE', #47827 ) ;
#24829=B_SPLINE_CURVE_WITH_KNOTS ( 'NONE', 3,
 ( #32696, #31703, #30702, #46931 ),
 .UNSPECIFIED., .F., .F.,
 ( 4, 4 ),
 ( 0.000000000000000000, 9.999999999998897304E-05 ),
 .UNSPECIFIED. ) ;
#24830=CARTESIAN_POINT ( 'NONE',  ( -22.77861398648627400, -3.026084143414268013, 11.49999999999998934 ) ) ;
#24832=EDGE_CURVE ( 'NONE', #18101, #87003, #37224, .T. ) ;
#24833=ORIENTED_EDGE ( 'NONE', *, *, #69873, .F. ) ;
#24836=EDGE_CURVE ( 'NONE', #48449, #67264, #9756, .T. ) ;
#24839=CARTESIAN_POINT ( 'NONE',  ( -29.62287095715004881, -24.58390616985635546, 1.056161279468100123 ) ) ;
#24840=CARTESIAN_POINT ( 'NONE',  ( -20.61954105445765251, -5.431428859615135885, 11.49999999999999645 ) ) ;
#24843=CARTESIAN_POINT ( 'NONE',  ( -4.073883676365832152, 21.86232641878667593, 11.49999999999998934 ) ) ;
#24844=CARTESIAN_POINT ( 'NONE',  ( 10.61356161029474521, 17.70173163822984819, -1.500000000000002220 ) ) ;
#24848=CARTESIAN_POINT ( 'NONE',  ( -95.54582827825265667, -24.73531770709095312, 8.716586749053508498 ) ) ;
#24849=VERTEX_POINT ( 'NONE', #41729 ) ;
#24850=DIRECTION ( 'NONE',  ( 0.000000000000000000, 2.173523156925980399E-06, -0.9999999999976378895 ) ) ;
#24852=VECTOR ( 'NONE', #95913, 1000.000000000000114 ) ;
#24853=CARTESIAN_POINT ( 'NONE',  ( -129.5895376238167387, -24.65952944569305316, 1.056160979905705011 ) ) ;
#24855=CARTESIAN_POINT ( 'NONE',  ( 13.94627346685978075, -15.57361473980792255, -1.500000000000002220 ) ) ;
#24856=CARTESIAN_POINT ( 'NONE',  ( -18.37375256118794553, 11.78967355450649457, 11.49999999999999645 ) ) ;
#24857=CARTESIAN_POINT ( 'NONE',  ( -27.07602811445854130, -24.77993765707372376, 7.457967602658744255 ) ) ;
#24858=CARTESIAN_POINT ( 'NONE',  ( -91.62287095715004170, -29.50248528299804818, 1.056150453629040253 ) ) ;
#24859=CARTESIAN_POINT ( 'NONE',  ( 22.08653571170524543, -4.319401766784854324, 11.49999999999998934 ) ) ;
#24860=CARTESIAN_POINT ( 'NONE',  ( -50.38822539166533687, -25.31296765081191680, 4.736250530724597674 ) ) ;
#24865=VERTEX_POINT ( 'NONE', #80779 ) ;
#24867=ORIENTED_EDGE ( 'NONE', *, *, #87362, .F. ) ;
#24868=CARTESIAN_POINT ( 'NONE',  ( -5.333777546869826303, -20.73983961313815172, -1.500000000000002220 ) ) ;
#24869=CARTESIAN_POINT ( 'NONE',  ( 13.15158565771796084, -18.08388448789661851, 11.49999999999999645 ) ) ;
#24872=CARTESIAN_POINT ( 'NONE',  ( -16.48755246578841849, -13.11705038010048163, 11.49999999999998934 ) ) ;
#24873=CARTESIAN_POINT ( 'NONE',  ( -30.50821306534034250, -24.04899441997164189, 10.47557002954947336 ) ) ;
#24874=CARTESIAN_POINT ( 'NONE',  ( -17.57349146297605103, 9.389787994052484876, -1.500000000000002220 ) ) ;
#24877=CARTESIAN_POINT ( 'NONE',  ( -18.24146354680218707, 12.35505607031776165, -1.500000000000002220 ) ) ;
#24878=CARTESIAN_POINT ( 'NONE',  ( -83.52287095715009002, -23.94994826722565406, -0.6494450866342720285 ) ) ;
#24880=CARTESIAN_POINT ( 'NONE',  ( -65.58377276114705978, -24.73531770709095312, 8.716586749053508498 ) ) ;
#24882=PLANE ( 'NONE',  #43267 ) ;
#24883=CARTESIAN_POINT ( 'NONE',  ( -1.025521031027718299, 20.81036885881322362, 11.49999999999999645 ) ) ;
#24884=CARTESIAN_POINT ( 'NONE',  ( -74.62287095715005592, -24.65952944569304606, 1.056160979905696351 ) ) ;
#24886=CARTESIAN_POINT ( 'NONE',  ( -129.5228709571500758, -23.47596703998600631, 11.44779298504227683 ) ) ;
#24887=LINE ( 'NONE', #25394, #88592 ) ;
#24888=CARTESIAN_POINT ( 'NONE',  ( -11.06822068739258391, -18.21809710261049275, 11.49999999999998934 ) ) ;
#24890=CARTESIAN_POINT ( 'NONE',  ( -41.26959558397305727, -29.50249893827660941, 7.338705366995167623 ) ) ;
#24891=CARTESIAN_POINT ( 'NONE',  ( -92.52287095715006160, -23.47593901973090169, -1.443836447538996426 ) ) ;
#24893=CARTESIAN_POINT ( 'NONE',  ( 22.48569338394020534, -0.9006126209707296937, -1.500000000000002220 ) ) ;
#24895=CARTESIAN_POINT ( 'NONE',  ( -83.55620429048340725, -24.66019654487199730, 8.947790411086126383 ) ) ;
#24896=ORIENTED_EDGE ( 'NONE', *, *, #65886, .F. ) ;
#24898=CARTESIAN_POINT ( 'NONE',  ( -119.5228709571500616, -24.66019654487200441, 8.947790411086108620 ) ) ;
#24899=CARTESIAN_POINT ( 'NONE',  ( -31.47681414363396613, -24.66019654487199020, 8.947790411086133489 ) ) ;
#24900=CARTESIAN_POINT ( 'NONE',  ( 11.88433821776028942, -15.71472908967258242, 11.49999999999999645 ) ) ;
#24902=PLANE ( 'NONE',  #65841 ) ;
#24903=ORIENTED_EDGE ( 'NONE', *, *, #94745, .F. ) ;
#24904=CARTESIAN_POINT ( 'NONE',  ( -99.63465086565865647, -23.73766607897671577, -1.055555164236429144 ) ) ;
#24906=CARTESIAN_POINT ( 'NONE',  ( -124.5904482984883970, -23.96169478059714564, 10.65365249895717170 ) ) ;
#24911=CARTESIAN_POINT ( 'NONE',  ( -9.637476322613308000, -17.25261889746210997, -1.500000000000002220 ) ) ;
#24913=EDGE_CURVE ( 'NONE', #30912, #2401, #33598, .T. ) ;
#24914=CARTESIAN_POINT ( 'NONE',  ( -14.69473627950705108, 13.90061564059656440, 11.49999999999999645 ) ) ;
#24918=CARTESIAN_POINT ( 'NONE',  ( -48.62287095715004881, -23.47596703998600276, 11.44779298504227505 ) ) ;
#24920=CARTESIAN_POINT ( 'NONE',  ( -51.52764846858840997, -25.24768739062223943, 6.187572788000800017 ) ) ;
#24925=CARTESIAN_POINT ( 'NONE',  ( -1.591348192139008466, -19.94584644712825039, 11.49999999999998934 ) ) ;
#24926=EDGE_CURVE ( 'NONE', #153, #96640, #50525, .T. ) ;
#24927=CARTESIAN_POINT ( 'NONE',  ( -99.92788026055190187, -25.27532880725036790, 2.920407968822682054 ) ) ;
#24928=CARTESIAN_POINT ( 'NONE',  ( -116.5185765065318861, -24.15620529776628800, 10.23563542870659759 ) ) ;
#24931=CARTESIAN_POINT ( 'NONE',  ( -79.62361068839391010, -24.66019654487199375, 8.947790411086119278 ) ) ;
#24932=CARTESIAN_POINT ( 'NONE',  ( -109.9559143002945234, -25.18430168171479266, 3.359997616863110270 ) ) ;
#24933=CARTESIAN_POINT ( 'NONE',  ( -35.58884038832008656, -24.52300882791529446, 0.6510814631126419227 ) ) ;
#24934=CARTESIAN_POINT ( 'NONE',  ( -100.5895376238167245, -23.48786465467241769, 11.44779295918254114 ) ) ;
#24935=CARTESIAN_POINT ( 'NONE',  ( -116.7735373858569119, -25.37153787860454202, 4.078969152973338730 ) ) ;
#24939=CARTESIAN_POINT ( 'NONE',  ( -49.62090859027108536, -25.22926554657857423, 3.641651233274940669 ) ) ;
#24940=ORIENTED_EDGE ( 'NONE', *, *, #32289, .F. ) ;
#24941=CARTESIAN_POINT ( 'NONE',  ( 16.59675031405745571, -11.69241480613374407, 11.49999999999998934 ) ) ;
#24944=CARTESIAN_POINT ( 'NONE',  ( -34.62918016310124614, -24.51314013834315375, 0.6176544820404091807 ) ) ;
#24945=CARTESIAN_POINT ( 'NONE',  ( -105.6228709571500559, -23.48783264082479150, -1.443836473390060160 ) ) ;
#24949=CARTESIAN_POINT ( 'NONE',  ( -9.895454706725905325, 17.58729670687104729, -1.500000000000002220 ) ) ;
#24951=VECTOR ( 'NONE', #32071, 1000.000000000000114 ) ;
#24952=CARTESIAN_POINT ( 'NONE',  ( -3.044128750896296420, -20.94304649679510888, 11.49999999999999645 ) ) ;
#24953=CARTESIAN_POINT ( 'NONE',  ( 17.03105324785762420, 14.15717209551829647, -1.500000000000002220 ) ) ;
#24955=CARTESIAN_POINT ( 'NONE',  ( -20.44794078217315558, 2.270689272194197805, 11.49999999999998934 ) ) ;
#24958=CARTESIAN_POINT ( 'NONE',  ( -88.55620429048339304, -23.47596703998600631, 11.44779298504227683 ) ) ;
#24959=VERTEX_POINT ( 'NONE', #58942 ) ;
#24960=CARTESIAN_POINT ( 'NONE',  ( -54.51466552200992055, -23.73766607897669800, -1.055555164236461785 ) ) ;
#24961=DIRECTION ( 'NONE',  ( -3.773278334453079030E-23, 0.9999999999976377785, 2.173523156925979128E-06 ) ) ;
#24964=VERTEX_POINT ( 'NONE', #3660 ) ;
#24965=CARTESIAN_POINT ( 'NONE',  ( -112.6228709571500417, -24.65952944569304961, 1.056160979905702346 ) ) ;
#24966=CARTESIAN_POINT ( 'NONE',  ( -105.6228709571500275, -25.00158670708909625, 2.256160236439166411 ) ) ;
#24968=CARTESIAN_POINT ( 'NONE',  ( -19.40401905104624802, 7.283777608679691262, -1.500000000000002220 ) ) ;
#24969=CARTESIAN_POINT ( 'NONE',  ( 17.85095790706337127, 12.24325521369631176, 11.49999999999999645 ) ) ;
#24970=ORIENTED_EDGE ( 'NONE', *, *, #83089, .F. ) ;
#24973=CARTESIAN_POINT ( 'NONE',  ( 6.968497804723354783, -21.30229754059623559, 11.49999999999998934 ) ) ;
#24974=CARTESIAN_POINT ( 'NONE',  ( -47.61502911968744201, -23.48786465467240347, 11.44779295918255002 ) ) ;
#24975=CARTESIAN_POINT ( 'NONE',  ( -53.52287095715006870, -24.64898659630367916, 1.056161002820821038 ) ) ;
#24976=ORIENTED_EDGE ( 'NONE', *, *, #32284, .T. ) ;
#24978=CARTESIAN_POINT ( 'NONE',  ( -120.6228709571500843, -24.15516710230294706, 10.28746687063725851 ) ) ;
#24979=ORIENTED_EDGE ( 'NONE', *, *, #100274, .T. ) ;
#24980=ORIENTED_EDGE ( 'NONE', *, *, #78848, .T. ) ;
#24981=FACE_OUTER_BOUND ( 'NONE', #68414, .T. ) ;
#24983=B_SPLINE_CURVE_WITH_KNOTS ( 'NONE', 3,
 ( #40846, #24116, #48974, #2805 ),
 .UNSPECIFIED., .F., .F.,
 ( 4, 4 ),
 ( 1.387778780781445676E-17, 9.999999999999593903E-05 ),
 .UNSPECIFIED. ) ;
#24984=CARTESIAN_POINT ( 'NONE',  ( -129.6228709571500417, -24.64965695001463430, 8.947790411086117501 ) ) ;
#24985=CARTESIAN_POINT ( 'NONE',  ( 10.81949470224598997, -18.29866561848832518, -1.500000000000002220 ) ) ;
#24986=EDGE_LOOP ( 'NONE', ( #73411, #37208, #40948, #18589 ) ) ;
#24987=CARTESIAN_POINT ( 'NONE',  ( -50.63517956937771203, -24.63355581998386157, 0.9682620441943928791 ) ) ;
#24988=CARTESIAN_POINT ( 'NONE',  ( 12.66963027563507005, -17.75133666976559255, -1.500000000000002220 ) ) ;
#24989=CARTESIAN_POINT ( 'NONE',  ( -52.62809792546378418, -24.51419770103158413, 9.386484678747189392 ) ) ;
#24992=CARTESIAN_POINT ( 'NONE',  ( -6.542779104410481494, 20.88585256366161502, -1.500000000000002220 ) ) ;
#24993=CARTESIAN_POINT ( 'NONE',  ( -30.57287095715006231, -24.66858702400017123, 1.114042296326039017 ) ) ;
#24995=CARTESIAN_POINT ( 'NONE',  ( -30.49303573129054357, -23.47596703998576118, 11.44779287168131710 ) ) ;
#24996=B_SPLINE_CURVE_WITH_KNOTS ( 'NONE', 3,
 ( #26315, #27807, #19187, #33928 ),
 .UNSPECIFIED., .F., .F.,
 ( 4, 4 ),
 ( 0.000000000000000000, 9.999999999999592548E-05 ),
 .UNSPECIFIED. ) ;
#24999=ORIENTED_EDGE ( 'NONE', *, *, #10549, .F. ) ;
#25000=ORIENTED_EDGE ( 'NONE', *, *, #76619, .F. ) ;
#25001=PLANE ( 'NONE',  #63771 ) ;
#25002=CARTESIAN_POINT ( 'NONE',  ( -82.58247902686774466, -24.65952944569304606, 1.056160979905702790 ) ) ;
#25003=B_SPLINE_CURVE_WITH_KNOTS ( 'NONE', 3,
 ( #74458, #42534, #49152, #49643, #73468, #65383 ),
 .UNSPECIFIED., .F., .F.,
 ( 4, 2, 4 ),
 ( 1.570887131794176733E-05, 0.001396322306279756519, 0.002776935741241571502 ),
 .UNSPECIFIED. ) ;
#25004=CARTESIAN_POINT ( 'NONE',  ( -3.247986963444697395, 20.98610878802851332, -1.500000000000002220 ) ) ;
#25006=LINE ( 'NONE', #90911, #83756 ) ;
#25007=AXIS2_PLACEMENT_3D ( 'NONE', #21792, #46156, #30419 ) ;
#25008=FACE_OUTER_BOUND ( 'NONE', #28917, .T. ) ;
#25009=B_SPLINE_CURVE_WITH_KNOTS ( 'NONE', 3,
 ( #68407, #59808, #99340, #45079, #99825, #90242, #92231, #22703, #52184, #20717, #90742, #6000, #28844, #29837, #67920, #21708 ),
 .UNSPECIFIED., .F., .F.,
 ( 4, 2, 2, 2, 2, 2, 2, 4 ),
 ( 0.000000000000000000, 0.0002659278985097128707, 0.0005318557970194257413, 0.0007977836955291387746, 0.001063711594038851483, 0.001595567391058279067, 0.001861495289568003376, 0.002127423188077727251 ),
 .UNSPECIFIED. ) ;
#25010=PLANE ( 'NONE',  #26535 ) ;
#25011=CARTESIAN_POINT ( 'NONE',  ( -5.977879402576776968, -18.46583800616800630, -1.500000000000002220 ) ) ;
#25012=FACE_OUTER_BOUND ( 'NONE', #75375, .T. ) ;
#25013=ORIENTED_EDGE ( 'NONE', *, *, #87049, .T. ) ;
#25015=CARTESIAN_POINT ( 'NONE',  ( 16.53150372360616771, 10.32350692489952593, 11.49999999999999645 ) ) ;
#25017=EDGE_CURVE ( 'NONE', #39724, #91631, #42098, .T. ) ;
#25022=CARTESIAN_POINT ( 'NONE',  ( -98.58953762381673869, -24.66019654487199375, 8.947790411086119278 ) ) ;
#25023=CARTESIAN_POINT ( 'NONE',  ( -32.52287095715006160, -23.48786465467240347, 11.44779295918255357 ) ) ;
#25026=B_SPLINE_CURVE_WITH_KNOTS ( 'NONE', 3,
 ( #77195, #31033, #7701, #69610 ),
 .UNSPECIFIED., .F., .F.,
 ( 4, 4 ),
 ( 0.000000000000000000, 9.999999999998897304E-05 ),
 .UNSPECIFIED. ) ;
#25027=B_SPLINE_CURVE_WITH_KNOTS ( 'NONE', 3,
 ( #98765, #52111, #83036, #13526, #46991, #69826 ),
 .UNSPECIFIED., .F., .F.,
 ( 4, 2, 4 ),
 ( 0.000000000000000000, 0.001380901958385386376, 0.002761803916770772752 ),
 .UNSPECIFIED. ) ;
#25028=CARTESIAN_POINT ( 'NONE',  ( -81.86427935766467101, -25.03155814569520743, 6.429953324065727394 ) ) ;
#25029=CARTESIAN_POINT ( 'NONE',  ( 18.74904333037421011, -5.873301551693434597, -1.500000000000002220 ) ) ;
#25030=ORIENTED_EDGE ( 'NONE', *, *, #78777, .T. ) ;
#25032=CARTESIAN_POINT ( 'NONE',  ( -114.6228709571500701, -23.47596703998600631, 11.44779298504227860 ) ) ;
#25034=EDGE_CURVE ( 'NONE', #100167, #83385, #35107, .T. ) ;
#25035=DIRECTION ( 'NONE',  ( 0.000000000000000000, -0.9999999999976377785, -2.173523156925979975E-06 ) ) ;
#25036=LINE ( 'NONE', #86937, #8534 ) ;
#25037=LINE ( 'NONE', #2224, #26619 ) ;
#25038=CARTESIAN_POINT ( 'NONE',  ( -101.5951766307233441, -25.13932753814477294, 7.067349521424753256 ) ) ;
#25040=CARTESIAN_POINT ( 'NONE',  ( -129.6239064868591981, -23.48783264082478084, -1.443836473390078590 ) ) ;
#25042=CARTESIAN_POINT ( 'NONE',  ( 11.38277053702107899, 16.36964821499295653, -1.500000000000002220 ) ) ;
#25043=CARTESIAN_POINT ( 'NONE',  ( -100.4326965455114902, -25.19502912051678578, 3.293943094755625633 ) ) ;
#25044=CARTESIAN_POINT ( 'NONE',  ( -18.24533751216517885, 7.751685665592884078, -1.500000000000002220 ) ) ;
#25045=ORIENTED_EDGE ( 'NONE', *, *, #46594, .F. ) ;
#25046=FACE_OUTER_BOUND ( 'NONE', #69527, .T. ) ;
#25047=B_SPLINE_CURVE_WITH_KNOTS ( 'NONE', 3,
 ( #94318, #51034, #71503, #63909, #56288, #40551 ),
 .UNSPECIFIED., .F., .F.,
 ( 4, 2, 4 ),
 ( 6.384118696095308626E-06, 0.001386860460837117774, 0.002767336802978140158 ),
 .UNSPECIFIED. ) ;
#25048=CARTESIAN_POINT ( 'NONE',  ( -50.73873594106601104, -25.13877094469005513, 7.069300430009204383 ) ) ;
#25051=CARTESIAN_POINT ( 'NONE',  ( -19.40401905104624802, 7.283777608679691262, 11.49999999999999645 ) ) ;
#25053=CARTESIAN_POINT ( 'NONE',  ( -106.5159538269883512, -24.15543982623907482, -0.2315651400026576268 ) ) ;
#25054=CARTESIAN_POINT ( 'NONE',  ( 18.64237364862239943, 13.12531859369229359, 11.49999999999999645 ) ) ;
#25055=ORIENTED_EDGE ( 'NONE', *, *, #87587, .F. ) ;
#25056=CARTESIAN_POINT ( 'NONE',  ( -57.62287095715004881, -23.48783264082478794, -1.443836473390068820 ) ) ;
#25057=DIRECTION ( 'NONE',  ( -1.000000000000000000, -3.773278334444167020E-23, -8.201307838832447938E-29 ) ) ;
#25058=ORIENTED_EDGE ( 'NONE', *, *, #62975, .F. ) ;
#25059=B_SPLINE_CURVE_WITH_KNOTS ( 'NONE', 3,
 ( #12597, #74496, #10855, #57046 ),
 .UNSPECIFIED., .F., .F.,
 ( 4, 4 ),
 ( 0.000000000000000000, 9.999999999998897304E-05 ),
 .UNSPECIFIED. ) ;
#25060=CARTESIAN_POINT ( 'NONE',  ( 14.71488472389458124, -13.84269218943631508, 11.49999999999998934 ) ) ;
#25062=CARTESIAN_POINT ( 'NONE',  ( -40.48088817674474882, -25.30533602047519892, 5.080586759489595039 ) ) ;
#25064=ORIENTED_EDGE ( 'NONE', *, *, #35351, .F. ) ;
#25065=CARTESIAN_POINT ( 'NONE',  ( -127.5228709571500616, -23.73907113216990794, -1.053371485793243467 ) ) ;
#25066=CARTESIAN_POINT ( 'NONE',  ( -51.62287095715007013, -23.96127896941632685, -0.6493128931037859264 ) ) ;
#25067=CARTESIAN_POINT ( 'NONE',  ( -12.72357806474857966, 15.40231687525621318, -1.500000000000002220 ) ) ;
#25068=CARTESIAN_POINT ( 'NONE',  ( -40.94687764114259920, -25.04307374350000259, 7.563175304812659761 ) ) ;
#25069=CARTESIAN_POINT ( 'NONE',  ( -4.092705237139750984, -20.55955383578756113, 11.49999999999999645 ) ) ;
#25071=CARTESIAN_POINT ( 'NONE',  ( -93.52287095715006160, -24.66019654487200086, 8.947790411086110396 ) ) ;
#25072=CARTESIAN_POINT ( 'NONE',  ( 20.91424602935089894, 6.983905699820807556, -1.500000000000002220 ) ) ;
#25074=AXIS2_PLACEMENT_3D ( 'NONE', #14065, #91198, #92688 ) ;
#25075=CARTESIAN_POINT ( 'NONE',  ( -101.6228709571500559, -23.47593901973091235, -1.443836447539001089 ) ) ;
#25076=ORIENTED_EDGE ( 'NONE', *, *, #32737, .T. ) ;
#25077=CARTESIAN_POINT ( 'NONE',  ( -60.52287095715005449, -24.14321612903115621, -0.2833117244521560774 ) ) ;
#25078=CARTESIAN_POINT ( 'NONE',  ( -49.51045894826389571, -25.18440238133807796, 3.920634963436217202 ) ) ;
#25079=PLANE ( 'NONE',  #41336 ) ;
#25080=VERTEX_POINT ( 'NONE', #7134 ) ;
#25081=CARTESIAN_POINT ( 'NONE',  ( -68.52287095715006160, -29.50250243563736774, 8.947779886222143375 ) ) ;
#25083=ORIENTED_EDGE ( 'NONE', *, *, #75083, .T. ) ;
#25086=DIRECTION ( 'NONE',  ( 0.000000000000000000, 2.173523156925980399E-06, -0.9999999999976378895 ) ) ;
#25087=CARTESIAN_POINT ( 'NONE',  ( 17.35315496411208613, -10.91789592880838811, -1.500000000000002220 ) ) ;
#25089=ORIENTED_EDGE ( 'NONE', *, *, #79261, .T. ) ;
#25090=CARTESIAN_POINT ( 'NONE',  ( -71.62287095715004170, -23.96177878511308990, 10.65340807706330217 ) ) ;
#25093=CARTESIAN_POINT ( 'NONE',  ( 3.885606641962014329, -21.97303888676646721, 11.49999999999998934 ) ) ;
#25094=CARTESIAN_POINT ( 'NONE',  ( -90.58953762381672448, -23.47593901973091235, -1.443836447539002865 ) ) ;
#25095=DIRECTION ( 'NONE',  ( -3.773278334444166432E-23, 1.000000000000000000, 0.000000000000000000 ) ) ;
#25096=ORIENTED_EDGE ( 'NONE', *, *, #21050, .F. ) ;
#25098=CARTESIAN_POINT ( 'NONE',  ( -73.52287095715007581, -23.73907113216989728, -1.053371485793252793 ) ) ;
#25100=CARTESIAN_POINT ( 'NONE',  ( -15.88994834598175387, -13.44966708658631838, -1.500000000000002220 ) ) ;
#25102=CARTESIAN_POINT ( 'NONE',  ( -116.5228709571500900, -24.51283580621456792, 0.6167428607047249489 ) ) ;
#25104=ORIENTED_EDGE ( 'NONE', *, *, #6973, .T. ) ;
#25105=CARTESIAN_POINT ( 'NONE',  ( -70.28247728326880406, -25.25935350244192534, 7.560916518431925581 ) ) ;
#25106=CARTESIAN_POINT ( 'NONE',  ( 1.225302832070333636, 21.05158420706169764, -1.500000000000002220 ) ) ;
#25108=CARTESIAN_POINT ( 'NONE',  ( -110.6228709571500701, -23.84047902841603062, -0.8780736468305480047 ) ) ;
#25110=CARTESIAN_POINT ( 'NONE',  ( -120.5169633428488254, -24.83644354573579349, 8.397322867130096569 ) ) ;
#25111=CARTESIAN_POINT ( 'NONE',  ( -101.8248201165894073, -25.03152257312019202, 6.680466978398867717 ) ) ;
#25112=CARTESIAN_POINT ( 'NONE',  ( -36.52287095715006870, -24.65952944569304606, 1.056160979905691910 ) ) ;
#25113=CARTESIAN_POINT ( 'NONE',  ( -127.6228709571500559, -29.50248528299804818, 1.056150453629047137 ) ) ;
#25114=CARTESIAN_POINT ( 'NONE',  ( -65.62287095715005592, -23.48786465467241058, 11.44779295918254647 ) ) ;
#25115=CARTESIAN_POINT ( 'NONE',  ( -15.96568504569681402, -15.38390974582250692, 11.49999999999999645 ) ) ;
#25116=VERTEX_POINT ( 'NONE', #44217 ) ;
#25117=CARTESIAN_POINT ( 'NONE',  ( -108.9228709571500531, -23.47593901973090169, -1.443836447538996648 ) ) ;
#25119=ORIENTED_EDGE ( 'NONE', *, *, #26672, .T. ) ;
#25120=CARTESIAN_POINT ( 'NONE',  ( 16.59953334139655468, -15.42474913338910980, 11.49999999999998934 ) ) ;
#25122=CARTESIAN_POINT ( 'NONE',  ( -125.6228709571500559, -29.50247984919015209, -1.443849546365044922 ) ) ;
#25123=VERTEX_POINT ( 'NONE', #69039 ) ;
#25124=ORIENTED_EDGE ( 'NONE', *, *, #49282, .T. ) ;
#25127=CARTESIAN_POINT ( 'NONE',  ( -17.16780662754360520, -10.58209718439171176, -1.500000000000002220 ) ) ;
#25129=ORIENTED_EDGE ( 'NONE', *, *, #4429, .T. ) ;
#25131=CARTESIAN_POINT ( 'NONE',  ( -130.5728709571500588, -24.88826271230664489, 8.528479341549758175 ) ) ;
#25132=CARTESIAN_POINT ( 'NONE',  ( -22.37156870845955225, 0.5457896250522937809, -1.500000000000002220 ) ) ;
#25133=VERTEX_POINT ( 'NONE', #21349 ) ;
#25135=CARTESIAN_POINT ( 'NONE',  ( -112.6283950228135495, -23.96169478059713498, 10.65365249895717348 ) ) ;
#25138=CARTESIAN_POINT ( 'NONE',  ( -40.29313279566920869, -25.31535333371619956, 5.078344701801774441 ) ) ;
#25142=CARTESIAN_POINT ( 'NONE',  ( -16.13938233076020268, 11.07636124087057183, 11.49999999999998934 ) ) ;
#25143=B_SPLINE_CURVE_WITH_KNOTS ( 'NONE', 3,
 ( #30945, #8116, #77608, #41959 ),
 .UNSPECIFIED., .F., .F.,
 ( 4, 4 ),
 ( 0.000000000000000000, 0.0001000000000000167422 ),
 .UNSPECIFIED. ) ;
#25144=ADVANCED_FACE ( 'NONE', ( #59949 ), #32859, .T. ) ;
#25145=FACE_OUTER_BOUND ( 'NONE', #31859, .T. ) ;
#25146=ORIENTED_EDGE ( 'NONE', *, *, #10972, .T. ) ;
#25147=CARTESIAN_POINT ( 'NONE',  ( 19.88731969966643476, 8.162773808193900749, -1.500000000000002220 ) ) ;
#25148=CARTESIAN_POINT ( 'NONE',  ( -128.5218876873007616, -23.96119346886882084, -0.6495511937831803806 ) ) ;
#25152=CARTESIAN_POINT ( 'NONE',  ( -80.62287095715005592, -24.91570333823099759, 8.075032458375547506 ) ) ;
#25153=CARTESIAN_POINT ( 'NONE',  ( -18.54830753475928518, 13.48922247889305837, -1.500000000000002220 ) ) ;
#25156=CARTESIAN_POINT ( 'NONE',  ( -103.5228709571500758, -23.47596703998600631, 11.44779298504228215 ) ) ;
#25158=CARTESIAN_POINT ( 'NONE',  ( -19.87929632332335927, 2.386914507623989490, 11.49999999999999645 ) ) ;
#25159=CARTESIAN_POINT ( 'NONE',  ( -26.09636659181000340, -24.96935267319560126, 4.940287552382958580 ) ) ;
#25160=CARTESIAN_POINT ( 'NONE',  ( -107.5895376238167387, -24.64898659630368272, 1.056161002820392270 ) ) ;
#25161=LINE ( 'NONE', #50027, #36049 ) ;
#25162=CARTESIAN_POINT ( 'NONE',  ( -103.5895376238167245, -24.64898659630368627, 1.056161002820392270 ) ) ;
#25163=EDGE_CURVE ( 'NONE', #45754, #44715, #6833, .T. ) ;
#25165=CARTESIAN_POINT ( 'NONE',  ( 5.644138345009856117, 19.01542066204735448, 11.49999999999998934 ) ) ;
#25167=CARTESIAN_POINT ( 'NONE',  ( -19.76859095128058996, -9.124614402804876789, 11.49999999999998934 ) ) ;
#25168=CARTESIAN_POINT ( 'NONE',  ( -90.62287095715001328, -24.83620972994592790, 8.398175272781360334 ) ) ;
#25169=CARTESIAN_POINT ( 'NONE',  ( 3.778003860535555702, 19.31821889988591323, -1.500000000000002220 ) ) ;
#25171=CARTESIAN_POINT ( 'NONE',  ( -42.66379183916900786, -23.48783264082477373, -1.443836473390076147 ) ) ;
#25174=DIRECTION ( 'NONE',  ( 3.773278334444166432E-23, -1.000000000000000000, 0.000000000000000000 ) ) ;
#25176=CARTESIAN_POINT ( 'NONE',  ( 15.34425395324244867, 13.73259486114767114, 11.49999999999999645 ) ) ;
#25177=PLANE ( 'NONE',  #16508 ) ;
#25178=CARTESIAN_POINT ( 'NONE',  ( -120.5880715386675064, -24.92564183028979485, 1.928384488918253092 ) ) ;
#25179=CARTESIAN_POINT ( 'NONE',  ( -9.785633969878258398, 20.35780147342342516, 11.49999999999999645 ) ) ;
#25180=VERTEX_POINT ( 'NONE', #8148 ) ;
#25181=LINE ( 'NONE', #17575, #57321 ) ;
#25182=CARTESIAN_POINT ( 'NONE',  ( -26.61313021603985263, -24.83282438599244912, 7.069134266065987937 ) ) ;
#25183=CARTESIAN_POINT ( 'NONE',  ( -97.63250698802460192, -23.96119346886881374, -0.6495511937832058047 ) ) ;
#25184=CARTESIAN_POINT ( 'NONE',  ( -72.62287095715005592, -23.47596703998600631, 11.44779298504227860 ) ) ;
#25185=ADVANCED_FACE ( 'NONE', ( #69550 ), #79147, .T. ) ;
#25187=CARTESIAN_POINT ( 'NONE',  ( -125.5228709571500616, -23.47596703998600631, 11.44779298504227683 ) ) ;
#25188=ADVANCED_FACE ( 'NONE', ( #78131 ), #41810, .T. ) ;
#25190=CARTESIAN_POINT ( 'NONE',  ( -79.36292229018619082, -25.26750046495177671, 5.750285965674462041 ) ) ;
#25191=CARTESIAN_POINT ( 'NONE',  ( 19.70479270790718829, 11.56945388388114360, -1.500000000000002220 ) ) ;
#25193=CARTESIAN_POINT ( 'NONE',  ( -106.6228709571500559, -23.48786465467241769, 11.44779295918253759 ) ) ;
#25194=CARTESIAN_POINT ( 'NONE',  ( -82.58519193231559541, -24.51419770103156281, 9.386484678747187615 ) ) ;
#25196=CARTESIAN_POINT ( 'NONE',  ( 14.32739804834607256, 17.34395043298086847, 11.49999999999999645 ) ) ;
#25199=B_SPLINE_CURVE_WITH_KNOTS ( 'NONE', 3,
 ( #46543, #30306, #14582, #69878, #60781, #68875 ),
 .UNSPECIFIED., .F., .F.,
 ( 4, 2, 4 ),
 ( 6.384118678617110714E-06, 0.001386860460828379755, 0.002767336802978142326 ),
 .UNSPECIFIED. ) ;
#25200=CARTESIAN_POINT ( 'NONE',  ( -15.43752342082821905, -15.63289427301443801, 11.49999999999998934 ) ) ;
#25201=DIRECTION ( 'NONE',  ( -3.773278334453079030E-23, 0.9999999999976377785, 2.173523156925979128E-06 ) ) ;
#25202=CARTESIAN_POINT ( 'NONE',  ( -34.53214318888519330, -24.51419770103156637, 9.386484678747176957 ) ) ;
#25203=CARTESIAN_POINT ( 'NONE',  ( -68.94185455919210881, -25.23897982886904856, 6.276681587599555634 ) ) ;
#25205=CARTESIAN_POINT ( 'NONE',  ( -48.48926359912356077, -24.51419770103156637, 9.386484678747178734 ) ) ;
#25207=DIRECTION ( 'NONE',  ( -3.773278334453079030E-23, 0.9999999999976377785, 2.173523156925979128E-06 ) ) ;
#25208=ORIENTED_EDGE ( 'NONE', *, *, #27811, .F. ) ;
#25209=CARTESIAN_POINT ( 'NONE',  ( -2.888065500968368227, -20.30684875360264741, 11.49999999999998934 ) ) ;
#25212=EDGE_LOOP ( 'NONE', ( #47571, #77357, #36674, #1173 ) ) ;
#25215=CARTESIAN_POINT ( 'NONE',  ( 8.651921485055520833, -21.43433228965458781, -1.500000000000002220 ) ) ;
#25216=CARTESIAN_POINT ( 'NONE',  ( -112.5228709571500616, -23.48786465467241769, 11.44779295918253936 ) ) ;
#25217=CARTESIAN_POINT ( 'NONE',  ( 13.61570878652767291, 15.11107311891478666, -1.500000000000002220 ) ) ;
#25218=ADVANCED_FACE ( 'NONE', ( #92869 ), #17448, .T. ) ;
#25220=FACE_OUTER_BOUND ( 'NONE', #70819, .T. ) ;
#25221=CARTESIAN_POINT ( 'NONE',  ( -92.50939861997672153, -24.34968618360935011, 0.1864209137778966296 ) ) ;
#25222=DIRECTION ( 'NONE',  ( 3.773278334444166432E-23, -1.000000000000000000, 0.000000000000000000 ) ) ;
#25223=CARTESIAN_POINT ( 'NONE',  ( -97.62287095715008434, -23.47596703998600631, 11.44779298504227860 ) ) ;
#25224=CARTESIAN_POINT ( 'NONE',  ( -7.189238790567602067, -20.27908067168375794, 11.49999999999999645 ) ) ;
#25226=CARTESIAN_POINT ( 'NONE',  ( -75.59183437362925417, -24.40034930558991633, 0.3402023900116103450 ) ) ;
#25227=CARTESIAN_POINT ( 'NONE',  ( -49.14050969713319716, -25.26385701502970704, 4.284284378226445256 ) ) ;
#25229=CARTESIAN_POINT ( 'NONE',  ( -15.27568272636907665, 14.01247568063241999, 11.49999999999998934 ) ) ;
#25230=VERTEX_POINT ( 'NONE', #87263 ) ;
#25232=CARTESIAN_POINT ( 'NONE',  ( -125.6240015775084942, -24.73486907724918638, 1.287355809206972346 ) ) ;
#25233=ORIENTED_EDGE ( 'NONE', *, *, #48249, .T. ) ;
#25234=AXIS2_PLACEMENT_3D ( 'NONE', #53422, #68644, #43811 ) ;
#25235=CARTESIAN_POINT ( 'NONE',  ( -86.62287095715001328, -23.73907113216991149, -1.053371485793227924 ) ) ;
#25236=CARTESIAN_POINT ( 'NONE',  ( -48.52287095715004739, -23.48783264083430211, -1.443836473375264440 ) ) ;
#25237=ORIENTED_EDGE ( 'NONE', *, *, #56277, .T. ) ;
#25238=EDGE_LOOP ( 'NONE', ( #75301, #17309, #86394, #94620 ) ) ;
#25241=DIRECTION ( 'NONE',  ( -0.000000000000000000, 2.173523156925979552E-06, -0.9999999999976378895 ) ) ;
#25242=VECTOR ( 'NONE', #4054, 1000.000000000000114 ) ;
#25243=CARTESIAN_POINT ( 'NONE',  ( -29.81066105410539535, -25.25535961780526861, 4.756373910324647625 ) ) ;
#25244=CARTESIAN_POINT ( 'NONE',  ( -5.411813039392390223, -21.34095290059367755, 11.49999999999999645 ) ) ;
#25245=ORIENTED_EDGE ( 'NONE', *, *, #92352, .F. ) ;
#25246=VECTOR ( 'NONE', #6484, 1000.000000000000114 ) ;
#25247=CARTESIAN_POINT ( 'NONE',  ( -103.6288243288032760, -24.15543982623907482, -0.2315651400026619011 ) ) ;
#25248=CARTESIAN_POINT ( 'NONE',  ( 0.2737972009257602091, 22.58959237946467624, -1.500000000000002220 ) ) ;
#25250=CARTESIAN_POINT ( 'NONE',  ( 17.94697546605861760, -10.91086909363634838, 11.49999999999998934 ) ) ;
#25251=CARTESIAN_POINT ( 'NONE',  ( -33.52287095715006160, -29.50250243563736774, 8.947779886222150481 ) ) ;
#25256=ORIENTED_EDGE ( 'NONE', *, *, #31267, .F. ) ;
#25257=CARTESIAN_POINT ( 'NONE',  ( -5.075574613727041218, 20.51645923614106337, 11.49999999999998934 ) ) ;
#25258=CARTESIAN_POINT ( 'NONE',  ( -66.62287095715009855, -24.50321055353805022, 9.387540953477525818 ) ) ;
#25259=CARTESIAN_POINT ( 'NONE',  ( -50.75822869421170225, -25.03148736841117739, 7.539273415008683976 ) ) ;
#25260=CARTESIAN_POINT ( 'NONE',  ( -75.62287095715008434, -24.82558206586144323, 1.605769216559443269 ) ) ;
#25263=CARTESIAN_POINT ( 'NONE',  ( 16.02632597834478645, 15.35701383120132313, -1.500000000000002220 ) ) ;
#25264=CARTESIAN_POINT ( 'NONE',  ( -114.6278450564630589, -23.96119346886881729, -0.6495511937831860427 ) ) ;
#25265=EDGE_CURVE ( 'NONE', #87961, #17471, #87898, .T. ) ;
#25266=ORIENTED_EDGE ( 'NONE', *, *, #22037, .T. ) ;
#25269=CARTESIAN_POINT ( 'NONE',  ( -1.608633542659107629, -19.34071428503001755, 11.49999999999999645 ) ) ;
#25270=CARTESIAN_POINT ( 'NONE',  ( -71.52287095715010423, -23.48783264082477018, -1.443836473390091246 ) ) ;
#25271=CARTESIAN_POINT ( 'NONE',  ( -100.4381051993576506, -25.11033443737754212, 2.832404817301930056 ) ) ;
#25272=CARTESIAN_POINT ( 'NONE',  ( 18.70946937610417038, -5.484834493922766896, 11.49999999999998934 ) ) ;
#25273=ADVANCED_FACE ( 'NONE', ( #33477 ), #80657, .F. ) ;
#25274=CARTESIAN_POINT ( 'NONE',  ( 19.99361899508246765, -7.638522130635823082, -1.500000000000002220 ) ) ;
#25276=CARTESIAN_POINT ( 'NONE',  ( -60.58905053272714269, -24.52399227489755518, 9.353111116819372128 ) ) ;
#25277=ADVANCED_FACE ( 'NONE', ( #3047 ), #56378, .T. ) ;
#25278=CARTESIAN_POINT ( 'NONE',  ( -116.5228709571500616, -29.50248528299804818, 1.056150453629045360 ) ) ;
#25280=CARTESIAN_POINT ( 'NONE',  ( 22.50852769316577096, -3.342225187595919689, -1.500000000000002220 ) ) ;
#25282=CARTESIAN_POINT ( 'NONE',  ( -102.5149031412999676, -24.15543982623908192, -0.2315651400026460249 ) ) ;
#25283=DIRECTION ( 'NONE',  ( 1.000000000000000000, 3.773278334444167608E-23, 8.201307833595939069E-29 ) ) ;
#25284=CARTESIAN_POINT ( 'NONE',  ( -19.08307359429613825, -5.530936995296134917, 11.49999999999999645 ) ) ;
#25285=CARTESIAN_POINT ( 'NONE',  ( -84.52287095715001897, -24.51283580621364067, 0.6167428607019780351 ) ) ;
#25286=CARTESIAN_POINT ( 'NONE',  ( -73.62287095715005592, -24.64898659630367916, 1.056161002820824368 ) ) ;
#25287=CARTESIAN_POINT ( 'NONE',  ( -61.64687923781919920, -29.50248939449842922, 2.947779886236309377 ) ) ;
#25288=EDGE_LOOP ( 'NONE', ( #39471, #48482, #88834, #10371 ) ) ;
#25289=EDGE_CURVE ( 'NONE', #71512, #41368, #11142, .T. ) ;
#25292=CARTESIAN_POINT ( 'NONE',  ( -63.62287095715004881, -23.48786465467241058, 11.44779295918254824 ) ) ;
#25293=CARTESIAN_POINT ( 'NONE',  ( -6.994818212361641585, 20.52682044044541598, -1.500000000000002220 ) ) ;
#25295=CARTESIAN_POINT ( 'NONE',  ( -12.17249226084429203, 15.20430173202493940, -1.500000000000002220 ) ) ;
#25296=AXIS2_PLACEMENT_3D ( 'NONE', #18187, #49160, #80086 ) ;
#25297=CARTESIAN_POINT ( 'NONE',  ( -61.62287095715004881, -24.64965695001468404, 8.947790433994185832 ) ) ;
#25298=ORIENTED_EDGE ( 'NONE', *, *, #79796, .T. ) ;
#25299=CARTESIAN_POINT ( 'NONE',  ( -4.163110563111144913, -19.98234244090558320, 11.49999999999999645 ) ) ;
#25300=PLANE ( 'NONE',  #73173 ) ;
#25301=B_SPLINE_CURVE_WITH_KNOTS ( 'NONE', 3,
 ( #21144, #44502, #36382, #68834 ),
 .UNSPECIFIED., .F., .F.,
 ( 4, 4 ),
 ( 0.000000000000000000, 0.0001000000000000167422 ),
 .UNSPECIFIED. ) ;
#25303=CARTESIAN_POINT ( 'NONE',  ( -104.6228709571500559, -23.48783264082478794, -1.443836473390062158 ) ) ;
#25304=ORIENTED_EDGE ( 'NONE', *, *, #14791, .T. ) ;
#25305=CARTESIAN_POINT ( 'NONE',  ( -0.07401571716935598233, -22.09180837669121544, 9.787827635114012992 ) ) ;
#25307=CARTESIAN_POINT ( 'NONE',  ( -39.04303308397306438, -25.27985266284889931, 4.215216948853407253 ) ) ;
#25308=AXIS2_PLACEMENT_3D ( 'NONE', #63184, #33216, #25095 ) ;
#25309=CARTESIAN_POINT ( 'NONE',  ( -49.27764846858840997, -25.31439483164234971, 6.145204854548993012 ) ) ;
#25315=CARTESIAN_POINT ( 'NONE',  ( -66.62364627127672634, -24.66019654487199375, 8.947790411086119278 ) ) ;
#25316=AXIS2_PLACEMENT_3D ( 'NONE', #23681, #6972, #45546 ) ;
#25318=CARTESIAN_POINT ( 'NONE',  ( 21.75294195941402364, -7.338126679257295670, 11.49999999999999645 ) ) ;
#25319=CARTESIAN_POINT ( 'NONE',  ( 19.47892149737544187, 11.75266795981601753, -1.500000000000002220 ) ) ;
#25323=CARTESIAN_POINT ( 'NONE',  ( -90.62618102488053751, -24.83618233451450763, 1.606449574219535492 ) ) ;
#25324=CARTESIAN_POINT ( 'NONE',  ( -49.52287095715007581, -24.34917612406836440, 0.1852690917426526029 ) ) ;
#25325=EDGE_CURVE ( 'NONE', #98147, #33008, #93996, .T. ) ;
#25326=CARTESIAN_POINT ( 'NONE',  ( -69.51616040274272734, -23.73791477778911485, 11.05961554403170766 ) ) ;
#25327=ADVANCED_FACE ( 'NONE', ( #22602 ), #34524, .T. ) ;
#25328=CARTESIAN_POINT ( 'NONE',  ( -49.30270511914022080, -25.31386613526229823, 5.220951978813658023 ) ) ;
#25329=CARTESIAN_POINT ( 'NONE',  ( -77.22287095715006444, -23.47596703998600631, 11.44779298504227860 ) ) ;
#25330=CARTESIAN_POINT ( 'NONE',  ( -99.09705801370142808, -25.31200589627714237, 5.399822298496539830 ) ) ;
#25332=CARTESIAN_POINT ( 'NONE',  ( 20.39576089869593289, -0.2533167397448486957, -1.500000000000002220 ) ) ;
#25334=ORIENTED_EDGE ( 'NONE', *, *, #99248, .F. ) ;
#25335=CARTESIAN_POINT ( 'NONE',  ( 0.2859537766682072601, -23.01552763051285666, -1.500000000000002220 ) ) ;
#25337=EDGE_LOOP ( 'NONE', ( #2546, #46932, #85262, #88897 ) ) ;
#25338=AXIS2_PLACEMENT_3D ( 'NONE', #59228, #45506, #21635 ) ;
#25339=CARTESIAN_POINT ( 'NONE',  ( -101.5895376238167245, -24.65952944569304606, 1.056160979905695907 ) ) ;
#25340=CARTESIAN_POINT ( 'NONE',  ( -64.58953762381672448, -24.66019654487199020, 8.947790411086133489 ) ) ;
#25342=CARTESIAN_POINT ( 'NONE',  ( -29.52287095715007581, -24.57618165405973087, 1.056161296257514870 ) ) ;
#25343=CARTESIAN_POINT ( 'NONE',  ( 19.98943718749924159, -7.363913660680385220, 11.49999999999999645 ) ) ;
#25346=CARTESIAN_POINT ( 'NONE',  ( -20.66209241242137296, -8.185968977665980972, -1.500000000000002220 ) ) ;
#25347=CARTESIAN_POINT ( 'NONE',  ( 14.23986175545555355, -14.96101607593195304, 11.49999999999998934 ) ) ;
#25348=ADVANCED_FACE ( 'NONE', ( #97380 ), #6409, .F. ) ;
#25352=CARTESIAN_POINT ( 'NONE',  ( -95.63174276445451483, -24.40133493613050319, 9.663955038902802386 ) ) ;
#25353=ORIENTED_EDGE ( 'NONE', *, *, #30758, .T. ) ;
#25354=CARTESIAN_POINT ( 'NONE',  ( -95.52287095715011844, -24.91544648472627088, 1.928969306349431090 ) ) ;
#25355=ORIENTED_EDGE ( 'NONE', *, *, #91821, .F. ) ;
#25356=CARTESIAN_POINT ( 'NONE',  ( -58.49786823486456200, -24.35071581493543036, 9.817618358456028815 ) ) ;
#25357=CARTESIAN_POINT ( 'NONE',  ( 15.14581745102402088, -14.33592658440916523, -1.500000000000002220 ) ) ;
#25358=CARTESIAN_POINT ( 'NONE',  ( -13.92312151449838531, -16.86485062357919773, 11.49999999999999645 ) ) ;
#25360=CARTESIAN_POINT ( 'NONE',  ( -83.62287095715005592, -29.50247984919015209, -1.443849546365053582 ) ) ;
#25361=CARTESIAN_POINT ( 'NONE',  ( -14.31525571501011207, 17.33968770572689166, -1.500000000000002220 ) ) ;
#25362=EDGE_CURVE ( 'NONE', #18132, #55233, #75844, .T. ) ;
#25368=ORIENTED_EDGE ( 'NONE', *, *, #29760, .F. ) ;
#25370=ORIENTED_EDGE ( 'NONE', *, *, #36199, .F. ) ;
#25371=CARTESIAN_POINT ( 'NONE',  ( -52.52205781783337102, -23.48783264082478794, -1.443836473390069708 ) ) ;
#25372=ORIENTED_EDGE ( 'NONE', *, *, #28255, .F. ) ;
#25374=CARTESIAN_POINT ( 'NONE',  ( -9.048234560742015375, 19.43086790383670603, -1.500000000000002220 ) ) ;
#25375=CARTESIAN_POINT ( 'NONE',  ( 19.81157572017019319, -10.35993776028809421, 11.49999999999999645 ) ) ;
#25379=CARTESIAN_POINT ( 'NONE',  ( -19.04630365209304799, -9.011775662611203330, -1.500000000000002220 ) ) ;
#25380=CARTESIAN_POINT ( 'NONE',  ( -30.46018077524497869, -23.77895705106414326, 10.97490056816818971 ) ) ;
#25381=CARTESIAN_POINT ( 'NONE',  ( -13.91458393394894166, 14.26456941660895339, -1.500000000000002220 ) ) ;
#25382=CARTESIAN_POINT ( 'NONE',  ( -50.47999461636793939, -24.83644354573578639, 8.397322867130096569 ) ) ;
#25383=VECTOR ( 'NONE', #26871, 1000.000000000000114 ) ;
#25384=CARTESIAN_POINT ( 'NONE',  ( -69.62287095715005592, -29.50248528299804818, 1.056150453629036701 ) ) ;
#25385=CARTESIAN_POINT ( 'NONE',  ( -8.753671783739276790, -20.25744411100385634, -1.500000000000002220 ) ) ;
#25386=ORIENTED_EDGE ( 'NONE', *, *, #35715, .F. ) ;
#25387=CARTESIAN_POINT ( 'NONE',  ( -116.5903548954868825, -24.15543982623908548, -0.2315651400026406959 ) ) ;
#25388=ADVANCED_FACE ( 'NONE', ( #100219 ), #77891, .T. ) ;
#25389=PLANE ( 'NONE',  #96783 ) ;
#25390=CARTESIAN_POINT ( 'NONE',  ( -2.238888094254589234, -20.74146561784671761, 11.49999999999999645 ) ) ;
#25392=CARTESIAN_POINT ( 'NONE',  ( -62.64211077482075041, -23.96169478059712432, 10.65365249895718414 ) ) ;
#25393=CARTESIAN_POINT ( 'NONE',  ( -54.62287095715005592, -29.50250243563736774, 8.947779886222146928 ) ) ;
#25394=CARTESIAN_POINT ( 'NONE',  ( -79.11611000704996854, -29.50248939449842922, 2.947779886236309377 ) ) ;
#25395=CARTESIAN_POINT ( 'NONE',  ( -14.93283513470682067, -15.21490397768744529, 11.49999999999998934 ) ) ;
#25396=DIRECTION ( 'NONE',  ( -3.773278334453079618E-23, 0.9999999999976377785, 2.173523156925978705E-06 ) ) ;
#25397=CARTESIAN_POINT ( 'NONE',  ( -124.5228709571500758, -24.33832256527049864, 0.1851278514138631481 ) ) ;
#25398=B_SPLINE_CURVE_WITH_KNOTS ( 'NONE', 3,
 ( #62009, #77204, #46781, #1616, #39659, #38658 ),
 .UNSPECIFIED., .F., .F.,
 ( 4, 2, 4 ),
 ( 1.571346490231738784E-05, 0.001397069180539135423, 0.002778424896175953149 ),
 .UNSPECIFIED. ) ;
#25399=EDGE_CURVE ( 'NONE', #3013, #49044, #57727, .T. ) ;
#25400=CARTESIAN_POINT ( 'NONE',  ( -96.52287095715006160, -23.73934037231757443, 11.05740245334328087 ) ) ;
#25402=CARTESIAN_POINT ( 'NONE',  ( 22.42242567092132433, 2.420433022335332751, -1.500000000000002220 ) ) ;
#25403=EDGE_CURVE ( 'NONE', #53678, #93213, #24983, .T. ) ;
#25404=CARTESIAN_POINT ( 'NONE',  ( -51.52287095715006870, -24.51387760970724372, 9.387446482453414731 ) ) ;
#25406=CARTESIAN_POINT ( 'NONE',  ( -35.62287095715006302, -24.83620972994591369, 8.398175272781365663 ) ) ;
#25407=CARTESIAN_POINT ( 'NONE',  ( -31.66886117127272371, -23.48786465467240347, 11.44779295918255535 ) ) ;
#25408=CARTESIAN_POINT ( 'NONE',  ( 18.28535361393070957, 7.309334553982634652, 11.49999999999999645 ) ) ;
#25411=EDGE_LOOP ( 'NONE', ( #10214, #29441, #26879, #88753 ) ) ;
#25412=ADVANCED_FACE ( 'NONE', ( #786 ), #33233, .F. ) ;
#25413=CARTESIAN_POINT ( 'NONE',  ( -44.52287095715006160, -23.47593901973090169, -1.443836447538997092 ) ) ;
#25414=CARTESIAN_POINT ( 'NONE',  ( -61.52287095715006160, -23.48786465467241058, 11.44779295918254824 ) ) ;
#25418=EDGE_CURVE ( 'NONE', #91672, #76346, #31095, .T. ) ;
#25419=LINE ( 'NONE', #9695, #57835 ) ;
#25420=CARTESIAN_POINT ( 'NONE',  ( 19.18382676146983457, -4.683391092530263755, -1.500000000000002220 ) ) ;
#25421=ORIENTED_EDGE ( 'NONE', *, *, #9954, .F. ) ;
#25423=CARTESIAN_POINT ( 'NONE',  ( -19.33604739795523741, 5.927148246271303655, 11.49999999999999645 ) ) ;
#25427=CARTESIAN_POINT ( 'NONE',  ( -80.60265468748725937, -25.30556074514798937, 4.974404013225617760 ) ) ;
#25428=CARTESIAN_POINT ( 'NONE',  ( -50.44873633328847262, -25.30399780216363226, 5.199041709259373256 ) ) ;
#25431=CARTESIAN_POINT ( 'NONE',  ( -31.52287095715006160, -23.47596703998600631, 11.44779298504229459 ) ) ;
#25432=CARTESIAN_POINT ( 'NONE',  ( 13.83478396660306942, -14.44641118834825910, 11.49999999999998934 ) ) ;
#25435=VERTEX_POINT ( 'NONE', #55087 ) ;
#25437=EDGE_CURVE ( 'NONE', #61918, #65344, #26262, .T. ) ;
#25438=CARTESIAN_POINT ( 'NONE',  ( -104.6228709571500843, -23.73934037231757799, 11.05740245334328442 ) ) ;
#25439=CARTESIAN_POINT ( 'NONE',  ( -33.62287095715006302, -23.73907113216990794, -1.053371485793237472 ) ) ;
#25441=CARTESIAN_POINT ( 'NONE',  ( -80.64675904551154417, -25.21083105912962807, 3.409327675794629808 ) ) ;
#25442=CARTESIAN_POINT ( 'NONE',  ( -101.7776484685884242, -25.26303730729093644, 3.986250639247583827 ) ) ;
#25445=CARTESIAN_POINT ( 'NONE',  ( -99.90788617779853098, -25.11539320716599732, 2.804431449967498491 ) ) ;
#25448=AXIS2_PLACEMENT_3D ( 'NONE', #93751, #25241, #77014 ) ;
#25449=CARTESIAN_POINT ( 'NONE',  ( 11.01437679584920026, 17.03896688766576517, 11.49999999999998934 ) ) ;
#25450=B_SPLINE_CURVE_WITH_KNOTS ( 'NONE', 3,
 ( #51597, #97760, #90645, #42502, #58217, #21125 ),
 .UNSPECIFIED., .F., .F.,
 ( 4, 2, 4 ),
 ( 6.391158118956848875E-06, 0.001387004593080777039, 0.002767618028042597225 ),
 .UNSPECIFIED. ) ;
#25451=CARTESIAN_POINT ( 'NONE',  ( -126.5228709571499763, -23.48783264082477018, -1.443836473390082142 ) ) ;
#25452=CARTESIAN_POINT ( 'NONE',  ( -127.6236462943679015, -24.51419770103158768, 9.386484678747160970 ) ) ;
#25453=CARTESIAN_POINT ( 'NONE',  ( -59.62768243989484063, -24.51419770103156281, 9.386484678747184063 ) ) ;
#25455=CARTESIAN_POINT ( 'NONE',  ( -30.47287095715007510, -23.47596703474403768, 11.44538124590455830 ) ) ;
#25456=CARTESIAN_POINT ( 'NONE',  ( -5.075574613727041218, 20.51645923614106337, 11.49999999999999645 ) ) ;
#25457=CARTESIAN_POINT ( 'NONE',  ( -5.973063517705734071, 21.31661749205449041, -1.500000000000002220 ) ) ;
#25458=CARTESIAN_POINT ( 'NONE',  ( -19.39287000742378453, 6.875061630626206011, -1.500000000000002220 ) ) ;
#25459=ADVANCED_FACE ( 'NONE', ( #57096 ), #2086, .T. ) ;
#25460=ORIENTED_EDGE ( 'NONE', *, *, #87977, .F. ) ;
#25461=CARTESIAN_POINT ( 'NONE',  ( -88.62287095715004170, -23.47596703998600631, 11.44779298504227860 ) ) ;
#25462=ORIENTED_EDGE ( 'NONE', *, *, #18771, .F. ) ;
#25463=DIRECTION ( 'NONE',  ( 0.000000000000000000, 0.9999999999976377785, 2.173523156925979128E-06 ) ) ;
#25464=DIRECTION ( 'NONE',  ( -3.773278334453079030E-23, 0.9999999999976377785, 2.173523156925979128E-06 ) ) ;
#25466=ORIENTED_EDGE ( 'NONE', *, *, #92775, .T. ) ;
#25468=CARTESIAN_POINT ( 'NONE',  ( -81.62287095715007013, -23.72773821059536559, 11.05748984161097503 ) ) ;
#25469=DIRECTION ( 'NONE',  ( -3.773278334453079030E-23, 0.9999999999976377785, 2.173523156925979128E-06 ) ) ;
#25471=CARTESIAN_POINT ( 'NONE',  ( -10.81534556030752725, -17.66751395530895152, -1.500000000000002220 ) ) ;
#25472=CARTESIAN_POINT ( 'NONE',  ( -10.04279811845843007, 19.21892966915218892, 11.49999999999999645 ) ) ;
#25473=VERTEX_POINT ( 'NONE', #9895 ) ;
#25474=EDGE_CURVE ( 'NONE', #60922, #88443, #38281, .T. ) ;
#25477=CARTESIAN_POINT ( 'NONE',  ( -109.5895376238167103, -23.48786465467242124, 11.44779295918253936 ) ) ;
#25478=CARTESIAN_POINT ( 'NONE',  ( 22.28251467978060063, -2.329348454117679879, -1.500000000000002220 ) ) ;
#25480=EDGE_CURVE ( 'NONE', #10565, #83385, #64924, .T. ) ;
#25481=CARTESIAN_POINT ( 'NONE',  ( -47.58715896144654778, -24.35071581493542325, 9.817618358456030592 ) ) ;
#25483=ORIENTED_EDGE ( 'NONE', *, *, #74075, .T. ) ;
#25486=B_SPLINE_CURVE_WITH_KNOTS ( 'NONE', 3,
 ( #22869, #53854, #15272, #59, #31002, #62465, #61969, #93395 ),
 .UNSPECIFIED., .F., .F.,
 ( 4, 2, 2, 4 ),
 ( 2.306480500801492503E-11, 0.003266960683657127180, 0.004900441013953289217, 0.006533921344249451688 ),
 .UNSPECIFIED. ) ;
#25487=B_SPLINE_SURFACE_WITH_KNOTS ( 'NONE', 3, 1, ( 
 ( #92105, #84494 ),
 ( #85487, #84989 ),
 ( #15474, #62676 ),
 ( #31200, #22572 ),
 ( #29714, #53067 ),
 ( #60682, #91604 ),
 ( #256, #62173 ),
 ( #93096, #14976 ),
 ( #23579, #77863 ),
 ( #79874, #48445 ),
 ( #64187, #71781 ),
 ( #88501, #65190 ),
 ( #8870, #70774 ),
 ( #41841, #9364 ),
 ( #26095, #96114 ),
 ( #26603, #63173 ),
 ( #39816, #95108 ),
 ( #25596, #63684 ),
 ( #57564, #72783 ) ),
 .UNSPECIFIED., .F., .F., .F.,
 ( 4, 1, 1, 1, 1, 1, 1, 1, 1, 1, 1, 1, 1, 1, 1, 1, 4 ),
 ( 2, 2 ),
 ( 0.000000000000000000, 0.07262534608343565457, 0.1419766113262349028, 0.2089849284189395640, 0.2739568703644438274, 0.3368893473968409547, 0.3987449534945883278, 0.4601158852788603260, 0.5208249225900263291, 0.5809944586324817806, 0.6401519276014631110, 0.6986224507562535102, 0.7572710809271603338, 0.8164266940046565058, 0.8762540482034655298, 0.9371652930625368194, 0.9999999999999998890 ),
 ( 0.000000000000000000, 1.000000000000000000 ),
 .UNSPECIFIED. ) ;
#25488=EDGE_CURVE ( 'NONE', #97694, #36363, #20139, .T. ) ;
#25492=CARTESIAN_POINT ( 'NONE',  ( -39.55620429048339304, -24.66019654487199020, 8.947790411086135265 ) ) ;
#25493=VERTEX_POINT ( 'NONE', #27130 ) ;
#25495=CARTESIAN_POINT ( 'NONE',  ( 21.23515499356076930, 0.7789969333488580006, -1.500000000000002220 ) ) ;
#25496=VERTEX_POINT ( 'NONE', #90515 ) ;
#25497=CARTESIAN_POINT ( 'NONE',  ( -100.9048517508088310, -25.13595419642503614, 7.026370735367747145 ) ) ;
#25499=CARTESIAN_POINT ( 'NONE',  ( -15.20188179817220231, 15.67080601223297442, 11.49999999999998934 ) ) ;
#25500=CARTESIAN_POINT ( 'NONE',  ( -52.53219595083381677, -24.66019654487198665, 8.947790411086131712 ) ) ;
#25501=DIRECTION ( 'NONE',  ( 0.000000000000000000, 0.9999999999976377785, 2.173523156925979975E-06 ) ) ;
#25503=CARTESIAN_POINT ( 'NONE',  ( -21.73523922981167189, -2.474665994198115726, -1.500000000000002220 ) ) ;
#25505=EDGE_LOOP ( 'NONE', ( #23657, #17506, #6450, #5647 ) ) ;
#25507=CARTESIAN_POINT ( 'NONE',  ( -85.54115924640903756, -24.83644354573578994, 8.397322867130101898 ) ) ;
#25509=VERTEX_POINT ( 'NONE', #28621 ) ;
#25511=EDGE_LOOP ( 'NONE', ( #94519, #66591, #35342, #97205 ) ) ;
#25512=EDGE_CURVE ( 'NONE', #82077, #79877, #39557, .T. ) ;
#25516=CARTESIAN_POINT ( 'NONE',  ( 21.11169859150035677, 2.410084449224629832, -1.500000000000002220 ) ) ;
#25517=CARTESIAN_POINT ( 'NONE',  ( -91.62287095715004170, -23.48783264082478794, -1.443836473390063713 ) ) ;
#25518=FACE_OUTER_BOUND ( 'NONE', #49351, .T. ) ;
#25519=EDGE_CURVE ( 'NONE', #97228, #39695, #65221, .T. ) ;
#25523=CARTESIAN_POINT ( 'NONE',  ( 19.05472526407214673, 3.605321472892077050, -1.500000000000002220 ) ) ;
#25524=CARTESIAN_POINT ( 'NONE',  ( -45.63955093759643233, -24.52300882791528380, 0.6510814631126234930 ) ) ;
#25526=CARTESIAN_POINT ( 'NONE',  ( 17.91360334016800593, 7.682165803940314674, 11.49999999999999645 ) ) ;
#25530=ORIENTED_EDGE ( 'NONE', *, *, #97089, .F. ) ;
#25534=CARTESIAN_POINT ( 'NONE',  ( -90.52287095715007581, -24.92579138211019085, 1.929029949965666457 ) ) ;
#25535=ADVANCED_FACE ( 'NONE', ( #11896 ), #80911, .T. ) ;
#25537=CARTESIAN_POINT ( 'NONE',  ( 2.289404864003111051, -19.52285375609543294, 11.49999999999998934 ) ) ;
#25538=ADVANCED_FACE ( 'NONE', ( #59585 ), #20495, .T. ) ;
#25540=CARTESIAN_POINT ( 'NONE',  ( -94.62287095715005592, -23.47593901973091235, -1.443836447539002865 ) ) ;
#25541=CARTESIAN_POINT ( 'NONE',  ( 21.06059016766346659, 9.494407541345388779, -1.500000000000002220 ) ) ;
#25543=CARTESIAN_POINT ( 'NONE',  ( -106.6228709571500559, -24.64965695001469115, 8.947790433994176951 ) ) ;
#25545=CARTESIAN_POINT ( 'NONE',  ( -105.5228709571500758, -23.48786465467241769, 11.44779295918253936 ) ) ;
#25546=CARTESIAN_POINT ( 'NONE',  ( -97.62542694680625743, -24.51419770103157703, 9.386484678747176957 ) ) ;
#25547=CARTESIAN_POINT ( 'NONE',  ( -119.5228709571500900, -23.72747288104470442, -1.053458166803224794 ) ) ;
#25548=CARTESIAN_POINT ( 'NONE',  ( -44.52287095715004739, -23.48783264082477018, -1.443836473390094577 ) ) ;
#25551=CARTESIAN_POINT ( 'NONE',  ( -16.79965634883036074, 10.71410036745690597, 11.49999999999998934 ) ) ;
#25552=CARTESIAN_POINT ( 'NONE',  ( -75.54002366634762211, -24.73531770709095312, 8.716586749053512051 ) ) ;
#25553=CARTESIAN_POINT ( 'NONE',  ( 16.46483878678964174, 11.07114234313464252, -1.500000000000002220 ) ) ;
#25555=VECTOR ( 'NONE', #83773, 1000.000000000000114 ) ;
#25557=CARTESIAN_POINT ( 'NONE',  ( -51.46098519185604658, -25.22106701273937901, 6.517326689665016382 ) ) ;
#25559=CARTESIAN_POINT ( 'NONE',  ( 2.677173591928626806, -20.63698567995287902, 11.49999999999999645 ) ) ;
#25560=CARTESIAN_POINT ( 'NONE',  ( -81.52213711276834829, -23.48783264082478084, -1.443836473390067043 ) ) ;
#25561=CARTESIAN_POINT ( 'NONE',  ( -106.5228709571500758, -24.66019654487200441, 8.947790411086112172 ) ) ;
#25562=CARTESIAN_POINT ( 'NONE',  ( 13.80103769381473811, 18.14473668730428813, 11.49999999999999645 ) ) ;
#25564=B_SPLINE_SURFACE_WITH_KNOTS ( 'NONE', 3, 1, ( 
 ( #36515, #57887 ),
 ( #65507, #49772 ),
 ( #90309, #27912 ),
 ( #20779, #19291 ),
 ( #80703, #88320 ),
 ( #11678, #4588 ),
 ( #5570, #82192 ),
 ( #28908, #58378 ),
 ( #66994, #42660 ),
 ( #58870, #73594 ),
 ( #89811, #51757 ),
 ( #4083, #66007 ),
 ( #51254, #35036 ),
 ( #82689, #36018 ),
 ( #42164, #12678 ),
 ( #27422, #43642 ),
 ( #50760, #81704 ),
 ( #12176, #74580 ),
 ( #13170, #44141 ),
 ( #75068, #67481 ),
 ( #51907, #7204 ),
 ( #68619, #6211 ),
 ( #84328, #44295 ),
 ( #20934, #13316 ),
 ( #76214, #7711 ),
 ( #14814, #75712 ),
 ( #100036, #30040 ) ),
 .UNSPECIFIED., .F., .F., .F.,
 ( 4, 1, 1, 1, 1, 1, 1, 1, 1, 1, 1, 1, 1, 1, 1, 1, 1, 1, 1, 1, 1, 1, 1, 1, 4 ),
 ( 2, 2 ),
 ( 0.000000000000000000, 0.06859462225874241037, 0.1332460424433008772, 0.1943125864682560267, 0.2512792231169660995, 0.3045134392563467185, 0.3542349066533245772, 0.4004805887739885661, 0.4434107549384916913, 0.4840148686163448510, 0.5232523007732025055, 0.5610423727283596618, 0.5979002393643991775, 0.6335184888561948835, 0.6683143511696510997, 0.7024956712863812403, 0.7366853535134572084, 0.7702931693607888430, 0.8034372550192488971, 0.8359129516660280812, 0.8684602457892899308, 0.9008465382431827262, 0.9334665246307074504, 0.9662575752981232835, 0.9999999999999998890 ),
 ( 0.000000000000000000, 1.000000000000000000 ),
 .UNSPECIFIED. ) ;
#25567=ORIENTED_EDGE ( 'NONE', *, *, #67803, .F. ) ;
#25568=CARTESIAN_POINT ( 'NONE',  ( 11.17094659993960803, -16.83544227557131023, 11.49999999999998934 ) ) ;
#25570=CARTESIAN_POINT ( 'NONE',  ( -49.62287095715005592, -24.65952944569304250, 1.056160979905693020 ) ) ;
#25572=CARTESIAN_POINT ( 'NONE',  ( -35.62287095715005592, -23.47596703998600276, 11.44779298504227505 ) ) ;
#25573=ORIENTED_EDGE ( 'NONE', *, *, #95650, .T. ) ;
#25575=CARTESIAN_POINT ( 'NONE',  ( -84.52287095715007581, -23.72773821059536914, 11.05748984161097503 ) ) ;
#25576=CARTESIAN_POINT ( 'NONE',  ( -8.876215969300202957, 17.89991547088461488, -1.500000000000002220 ) ) ;
#25578=CARTESIAN_POINT ( 'NONE',  ( -0.6469382494902750080, 20.97623560764392181, 11.49999999999999645 ) ) ;
#25579=CARTESIAN_POINT ( 'NONE',  ( -29.03377166159867784, -24.89244382712345427, 7.705026311424929553 ) ) ;
#25580=CARTESIAN_POINT ( 'NONE',  ( -70.57802021803216519, -25.00182538069146787, 7.747789668545044250 ) ) ;
#25581=CARTESIAN_POINT ( 'NONE',  ( 10.81757466760856801, -19.22619917341675588, -1.500000000000002220 ) ) ;
#25586=DIRECTION ( 'NONE',  ( 3.773278334444166432E-23, -1.000000000000000000, 0.000000000000000000 ) ) ;
#25587=CARTESIAN_POINT ( 'NONE',  ( -72.50702299863668543, -24.15543982623907127, -0.2315651400026662310 ) ) ;
#25588=EDGE_LOOP ( 'NONE', ( #53806, #11124, #58085, #72958 ) ) ;
#25593=EDGE_CURVE ( 'NONE', #46066, #93369, #69681, .T. ) ;
#25594=ORIENTED_EDGE ( 'NONE', *, *, #50600, .T. ) ;
#25596=CARTESIAN_POINT ( 'NONE',  ( -100.4784170818037552, -25.27404630553893483, 2.833155736553538695 ) ) ;
#25598=CARTESIAN_POINT ( 'NONE',  ( -15.16157141410761966, -13.82251119679066953, -1.500000000000002220 ) ) ;
#25599=EDGE_CURVE ( 'NONE', #6180, #28046, #11691, .T. ) ;
#25603=CARTESIAN_POINT ( 'NONE',  ( -59.52287095715006160, -29.50250243563736774, 8.947779886222145151 ) ) ;
#25604=CARTESIAN_POINT ( 'NONE',  ( -22.22805510923732086, 2.117028069546627922, -1.500000000000002220 ) ) ;
#25606=EDGE_CURVE ( 'NONE', #11920, #80847, #79445, .T. ) ;
#25607=CARTESIAN_POINT ( 'NONE',  ( -81.62287095715005592, -24.64898659630528854, 1.056161002820826145 ) ) ;
#25609=ORIENTED_EDGE ( 'NONE', *, *, #53445, .T. ) ;
#25613=CARTESIAN_POINT ( 'NONE',  ( 2.550444227103870531, -20.70361394434535285, 11.49999999999998934 ) ) ;
#25615=PLANE ( 'NONE',  #55205 ) ;
#25617=VERTEX_POINT ( 'NONE', #38719 ) ;
#25619=CARTESIAN_POINT ( 'NONE',  ( -14.29351441246084065, -15.47709782942846424, -1.500000000000002220 ) ) ;
#25620=VERTEX_POINT ( 'NONE', #51965 ) ;
#25621=CARTESIAN_POINT ( 'NONE',  ( -110.6228709571500559, -23.47593901973091235, -1.443836447538999312 ) ) ;
#25623=DIRECTION ( 'NONE',  ( 0.000000000000000000, -0.9999999999976377785, -2.173523156925979128E-06 ) ) ;
#25624=CARTESIAN_POINT ( 'NONE',  ( -86.56264435747982589, -23.48786465467241058, 11.44779295918254647 ) ) ;
#25626=CARTESIAN_POINT ( 'NONE',  ( 15.89274262425319861, 14.76810421718133171, -1.500000000000002220 ) ) ;
#25627=CARTESIAN_POINT ( 'NONE',  ( -64.52287095715009002, -23.95044443724992078, 10.65354141964649592 ) ) ;
#25628=CARTESIAN_POINT ( 'NONE',  ( 12.24756355222007898, 18.56953561607567238, 11.49999999999999645 ) ) ;
#25629=ORIENTED_EDGE ( 'NONE', *, *, #4084, .T. ) ;
#25630=CARTESIAN_POINT ( 'NONE',  ( -51.11433842476665035, -25.31441771568657018, 5.424622361140696292 ) ) ;
#25631=EDGE_CURVE ( 'NONE', #95103, #100181, #98852, .T. ) ;
#25632=CARTESIAN_POINT ( 'NONE',  ( -71.27633360938686735, -25.26738409628678639, 5.967369320731084059 ) ) ;
#25634=CARTESIAN_POINT ( 'NONE',  ( -118.6228709571500701, -23.95044443724993144, 10.65354141964649415 ) ) ;
#25635=ORIENTED_EDGE ( 'NONE', *, *, #95955, .F. ) ;
#25639=CARTESIAN_POINT ( 'NONE',  ( -15.35229381799144299, -13.07563953244551591, -1.500000000000002220 ) ) ;
#25640=CARTESIAN_POINT ( 'NONE',  ( -126.5228709571500616, -23.47596703998600631, 11.44779298504227683 ) ) ;
#25642=CARTESIAN_POINT ( 'NONE',  ( -130.5728709571500872, -24.41126829859231151, 0.1249348357876886167 ) ) ;
#25643=CARTESIAN_POINT ( 'NONE',  ( 22.22467975111640470, 2.813832150844377100, -1.500000000000002220 ) ) ;
#25644=EDGE_LOOP ( 'NONE', ( #7437, #82885, #44973, #87794 ) ) ;
#25645=ORIENTED_EDGE ( 'NONE', *, *, #42286, .F. ) ;
#25648=CARTESIAN_POINT ( 'NONE',  ( -61.52287095715006870, -23.95044443724991368, 10.65354141964649415 ) ) ;
#25649=CARTESIAN_POINT ( 'NONE',  ( -125.5228709571500616, -24.63287334234355441, 0.9662140553097673390 ) ) ;
#25651=CARTESIAN_POINT ( 'NONE',  ( -130.5728709571500588, -24.66459861931857134, 1.095224832288509420 ) ) ;
#25652=EDGE_CURVE ( 'NONE', #7215, #7141, #58980, .T. ) ;
#25653=CARTESIAN_POINT ( 'NONE',  ( -16.69004703121433408, -10.21020960635683394, 11.49999999999998934 ) ) ;
#25654=CARTESIAN_POINT ( 'NONE',  ( -46.61531915723985264, -23.48783264082476663, -1.443836473390096575 ) ) ;
#25655=ORIENTED_EDGE ( 'NONE', *, *, #8362, .T. ) ;
#25656=CARTESIAN_POINT ( 'NONE',  ( -14.35963886870962192, 16.04489112172382903, -1.500000000000002220 ) ) ;
#25658=CARTESIAN_POINT ( 'NONE',  ( -71.26594616156928907, -25.12219007819659566, 6.471658164502055222 ) ) ;
#25659=CARTESIAN_POINT ( 'NONE',  ( -50.52287095715006160, -29.50248789122583659, 2.256150453626215580 ) ) ;
#25662=CARTESIAN_POINT ( 'NONE',  ( 19.54225192528841859, -11.95493969655435151, -1.500000000000002220 ) ) ;
#25665=CARTESIAN_POINT ( 'NONE',  ( -71.25889396629347061, -25.28176302922261343, 5.910822557617488648 ) ) ;
#25666=CARTESIAN_POINT ( 'NONE',  ( -13.75281105048956576, 14.62798779934380811, 11.49999999999999645 ) ) ;
#25672=CARTESIAN_POINT ( 'NONE',  ( -65.58953762381672448, -23.47593901973091235, -1.443836447539006196 ) ) ;
#25673=CARTESIAN_POINT ( 'NONE',  ( -4.880483578727112359, 19.22116399702514045, 11.49999999999998934 ) ) ;
#25674=CARTESIAN_POINT ( 'NONE',  ( -94.52287095715007581, -24.33927499327854349, 9.819080762295815390 ) ) ;
#25675=CARTESIAN_POINT ( 'NONE',  ( -2.223759785643201869, -19.53228827767608777, -1.500000000000002220 ) ) ;
#25677=AXIS2_PLACEMENT_3D ( 'NONE', #79208, #40665, #74111 ) ;
#25678=CARTESIAN_POINT ( 'NONE',  ( -41.62287095715007013, -23.96177878511307924, 10.65340807706330928 ) ) ;
#25680=CARTESIAN_POINT ( 'NONE',  ( -60.52287095715006870, -24.62285846331436545, 9.038163153548243400 ) ) ;
#25681=CARTESIAN_POINT ( 'NONE',  ( -39.06126217483156182, -25.29335695875766987, 4.454111424760057503 ) ) ;
#25682=CARTESIAN_POINT ( 'NONE',  ( 20.52162115075873672, 2.272738508513782119, 11.49999999999999645 ) ) ;
#25685=CARTESIAN_POINT ( 'NONE',  ( -22.43363504178351775, 2.973318333978472339, 11.49999999999999645 ) ) ;
#25686=ORIENTED_EDGE ( 'NONE', *, *, #13837, .F. ) ;
#25687=( NAMED_UNIT ( * ) SI_UNIT ( $, .STERADIAN. ) SOLID_ANGLE_UNIT ( ) );
#25688=CARTESIAN_POINT ( 'NONE',  ( -69.45438311041971247, -25.12219042273241953, 6.630173073956423302 ) ) ;
#25689=CARTESIAN_POINT ( 'NONE',  ( -45.52287095715006160, -29.50248528299804818, 1.056150453629033370 ) ) ;
#25690=CARTESIAN_POINT ( 'NONE',  ( -97.51109013237558543, -24.34968618360934300, 0.1864209137778855829 ) ) ;
#25691=CARTESIAN_POINT ( 'NONE',  ( -39.62287095715004170, -24.50216790748098461, 0.6166512839513541566 ) ) ;
#25692=CARTESIAN_POINT ( 'NONE',  ( -110.5228709571500616, -23.48783264082477018, -1.443836473390086583 ) ) ;
#25693=CARTESIAN_POINT ( 'NONE',  ( -28.52287095715007226, -24.35281102363228811, 9.387565062279906059 ) ) ;
#25696=CARTESIAN_POINT ( 'NONE',  ( -16.39533425382319720, 15.89506036719111037, -1.500000000000002220 ) ) ;
#25697=CARTESIAN_POINT ( 'NONE',  ( -110.4032350430226614, -25.18518318255442523, 3.295734047008243905 ) ) ;
#25698=CARTESIAN_POINT ( 'NONE',  ( -106.6228709571500275, -24.51387760970725083, 9.387446482453409402 ) ) ;
#25699=CARTESIAN_POINT ( 'NONE',  ( -63.49956169734852551, -24.35071581493543036, 9.817618358456027039 ) ) ;
#25700=CARTESIAN_POINT ( 'NONE',  ( 20.52096793114426276, -9.243637136814692568, 11.49999999999999645 ) ) ;
#25702=CARTESIAN_POINT ( 'NONE',  ( -78.52287095715006160, -29.50248528299804818, 1.056150453629038477 ) ) ;
#25703=CARTESIAN_POINT ( 'NONE',  ( 21.77894307773758698, -2.757304969434911879, 11.49999999999998934 ) ) ;
#25704=CARTESIAN_POINT ( 'NONE',  ( -114.5228709571500616, -24.64965694238408034, 8.947790433994192938 ) ) ;
#25705=CARTESIAN_POINT ( 'NONE',  ( -34.54551871025724807, -24.15620529776627379, 10.23563542870661003 ) ) ;
#25706=CARTESIAN_POINT ( 'NONE',  ( -69.88946996337978135, -25.04737768561031785, 7.495009054863854381 ) ) ;
#25707=ORIENTED_EDGE ( 'NONE', *, *, #6354, .F. ) ;
#25709=LINE ( 'NONE', #95228, #85070 ) ;
#25711=CARTESIAN_POINT ( 'NONE',  ( -54.59888109123160405, -23.96169478059712787, 10.65365249895718947 ) ) ;
#25712=EDGE_CURVE ( 'NONE', #5913, #84492, #75777, .T. ) ;
#25713=CARTESIAN_POINT ( 'NONE',  ( 20.39306652673287701, -2.074774109220689500, -1.500000000000002220 ) ) ;
#25714=ORIENTED_EDGE ( 'NONE', *, *, #55908, .T. ) ;
#25716=VERTEX_POINT ( 'NONE', #6769 ) ;
#25717=ORIENTED_EDGE ( 'NONE', *, *, #24095, .F. ) ;
#25718=ORIENTED_EDGE ( 'NONE', *, *, #39975, .F. ) ;
#25720=CARTESIAN_POINT ( 'NONE',  ( -5.338719972479099241, 22.46511350730333589, -1.500000000000002220 ) ) ;
#25721=DIRECTION ( 'NONE',  ( -3.773278334453079618E-23, 0.9999999999976377785, 2.173523156925979975E-06 ) ) ;
#25722=CARTESIAN_POINT ( 'NONE',  ( 2.178911383790714584, -20.24183328246387958, -1.500000000000002220 ) ) ;
#25724=VERTEX_POINT ( 'NONE', #93498 ) ;
#25727=CARTESIAN_POINT ( 'NONE',  ( -50.46347206883352499, -25.12095147923715643, 2.834909179762350906 ) ) ;
#25729=PLANE ( 'NONE',  #98263 ) ;
#25731=CARTESIAN_POINT ( 'NONE',  ( 14.33184905138074683, -16.10332302735202958, 11.49999999999999645 ) ) ;
#25733=CARTESIAN_POINT ( 'NONE',  ( -28.74075323809458737, -25.21531770609978906, 2.791732177081652555 ) ) ;
#25734=CARTESIAN_POINT ( 'NONE',  ( -43.62287095715003460, -23.47596703998600276, 11.44779298504227505 ) ) ;
#25739=EDGE_CURVE ( 'NONE', #7414, #71653, #46844, .T. ) ;
#25740=CARTESIAN_POINT ( 'NONE',  ( -5.109682455881146446, -20.12422286529520932, 11.49999999999998934 ) ) ;
#25742=CARTESIAN_POINT ( 'NONE',  ( -125.5209409955973854, -24.15503026093915295, -0.2815557561904348804 ) ) ;
#25743=VERTEX_POINT ( 'NONE', #17894 ) ;
#25744=CARTESIAN_POINT ( 'NONE',  ( -77.52287095715009002, -23.72747288104470087, -1.053458166803226792 ) ) ;
#25745=CARTESIAN_POINT ( 'NONE',  ( -38.62287095715005592, -29.50250243563736774, 8.947779886222148704 ) ) ;
#25746=ORIENTED_EDGE ( 'NONE', *, *, #82080, .T. ) ;
#25752=CARTESIAN_POINT ( 'NONE',  ( -11.61111146657235871, -18.70866699758865792, 11.49999999999999645 ) ) ;
#25753=ORIENTED_EDGE ( 'NONE', *, *, #70134, .F. ) ;
#25754=CARTESIAN_POINT ( 'NONE',  ( -103.5114003720115221, -24.51314013834316086, 0.6176544820404170633 ) ) ;
#25755=CARTESIAN_POINT ( 'NONE',  ( 15.88279217892459094, 16.07415641707351384, -1.500000000000002220 ) ) ;
#25756=EDGE_CURVE ( 'NONE', #23622, #98743, #74592, .T. ) ;
#25758=ORIENTED_EDGE ( 'NONE', *, *, #48524, .F. ) ;
#25759=ORIENTED_EDGE ( 'NONE', *, *, #59915, .F. ) ;
#25760=DIRECTION ( 'NONE',  ( 1.000000000000000000, 3.773278334444166432E-23, 8.201307841325785021E-29 ) ) ;
#25762=CARTESIAN_POINT ( 'NONE',  ( -57.48874627035196028, -24.66019654487198665, 8.947790411086121054 ) ) ;
#25764=CARTESIAN_POINT ( 'NONE',  ( -14.79452276021403634, 15.15755283273500531, 11.49999999999998934 ) ) ;
#25765=CARTESIAN_POINT ( 'NONE',  ( -82.62287095715007013, -23.96127896941631619, -0.6493128931037839280 ) ) ;
#25768=CARTESIAN_POINT ( 'NONE',  ( -41.33134938142555370, -25.30281732168844044, 5.289835615799674429 ) ) ;
#25769=CARTESIAN_POINT ( 'NONE',  ( 22.20243239366838850, -0.07139729354238147363, -1.500000000000002220 ) ) ;
#25770=CARTESIAN_POINT ( 'NONE',  ( -74.62287095715004170, -23.95044443724992789, 10.65354141964649415 ) ) ;
#25773=LINE ( 'NONE', #12040, #75153 ) ;
#25774=CARTESIAN_POINT ( 'NONE',  ( 14.52268490272241408, 12.84546865777419455, 11.49999999999999645 ) ) ;
#25775=CARTESIAN_POINT ( 'NONE',  ( -36.60923577182816757, -23.73791477778911130, 11.05961554403171121 ) ) ;
#25776=CARTESIAN_POINT ( 'NONE',  ( -116.5228709571500616, -24.64898659630368627, 1.056161002820833028 ) ) ;
#25777=CARTESIAN_POINT ( 'NONE',  ( 19.19537281719634336, 3.394423509666608663, 11.49999999999998934 ) ) ;
#25778=CARTESIAN_POINT ( 'NONE',  ( 6.029407872858970840, -20.54391778677962677, 11.49999999999998934 ) ) ;
#25779=CARTESIAN_POINT ( 'NONE',  ( -85.52287095715006160, -24.51254535375845833, 9.355368624242183628 ) ) ;
#25780=CARTESIAN_POINT ( 'NONE',  ( -108.5228709571500616, -29.50250243563736774, 8.947779886222136270 ) ) ;
#25781=CARTESIAN_POINT ( 'NONE',  ( -51.52205508352526664, -23.48783264082476308, -1.443836473390094133 ) ) ;
#25782=LINE ( 'NONE', #5437, #11733 ) ;
#25783=CARTESIAN_POINT ( 'NONE',  ( -20.99730734726578874, -8.693733401623333634, -1.500000000000002220 ) ) ;
#25784=ADVANCED_FACE ( 'NONE', ( #33115 ), #63079, .F. ) ;
#25786=CARTESIAN_POINT ( 'NONE',  ( -98.55008637382228187, -24.34968618360934300, 0.1864209137778828629 ) ) ;
#25787=CARTESIAN_POINT ( 'NONE',  ( -80.52287095715006160, -24.91544648472620338, 1.928969306349231028 ) ) ;
#25788=CARTESIAN_POINT ( 'NONE',  ( 17.36586316225375981, 9.700842922841564686, 11.49999999999999645 ) ) ;
#25789=CARTESIAN_POINT ( 'NONE',  ( -123.5552286427682986, -24.15620529776629510, 10.23563542870659404 ) ) ;
#25792=CARTESIAN_POINT ( 'NONE',  ( -67.62287095715005592, -24.65952944569304606, 1.056160979905697017 ) ) ;
#25796=EDGE_CURVE ( 'NONE', #96494, #59593, #85555, .T. ) ;
#25797=CARTESIAN_POINT ( 'NONE',  ( -31.22207807101783317, -25.16370864782812689, 7.203858152271859439 ) ) ;
#25798=CARTESIAN_POINT ( 'NONE',  ( -51.69862270353959843, -25.10935997717551160, 3.939198411942864020 ) ) ;
#25799=CARTESIAN_POINT ( 'NONE',  ( -19.97641003480726241, 8.421946895145676848, 11.49999999999998934 ) ) ;
#25802=CARTESIAN_POINT ( 'NONE',  ( -18.83898130102433299, -4.906684326670742280, -1.500000000000002220 ) ) ;
#25804=EDGE_LOOP ( 'NONE', ( #55998, #14623, #24369, #89650 ) ) ;
#25806=CARTESIAN_POINT ( 'NONE',  ( -51.52287095715005449, -24.66019654487199375, 8.947790411086119278 ) ) ;
#25807=CARTESIAN_POINT ( 'NONE',  ( -13.67433444753018534, -15.09191755960682890, 11.49999999999999645 ) ) ;
#25810=CARTESIAN_POINT ( 'NONE',  ( -89.52287095715006160, -24.64898659630528854, 1.056161002820827921 ) ) ;
#25811=ORIENTED_EDGE ( 'NONE', *, *, #93765, .F. ) ;
#25812=CARTESIAN_POINT ( 'NONE',  ( -62.62287095715003460, -23.73907113216991505, -1.053371485793230811 ) ) ;
#25813=CARTESIAN_POINT ( 'NONE',  ( -116.6228709571500275, -23.47596703998600631, 11.44779298504227860 ) ) ;
#25814=FACE_OUTER_BOUND ( 'NONE', #28850, .T. ) ;
#25816=CARTESIAN_POINT ( 'NONE',  ( -49.40320226356282518, -25.31439389004907525, 5.711994248101696314 ) ) ;
#25818=CARTESIAN_POINT ( 'NONE',  ( -109.6276325182596878, -24.15543982623907482, -0.2315651400026587092 ) ) ;
#25820=CARTESIAN_POINT ( 'NONE',  ( -42.52287095715005449, -24.65952944569303895, 1.056160979905691910 ) ) ;
#25821=CARTESIAN_POINT ( 'NONE',  ( 1.269710630819723463, 22.90746787927615102, 11.49999999999999645 ) ) ;
#25822=CARTESIAN_POINT ( 'NONE',  ( 15.01325480956343483, 17.08929600257393489, 11.49999999999998934 ) ) ;
#25825=CARTESIAN_POINT ( 'NONE',  ( -90.63103312429373659, -24.52300882791528380, 0.6510814631126311536 ) ) ;
#25826=CARTESIAN_POINT ( 'NONE',  ( -54.62287095715005592, -23.48786465467240347, 11.44779295918255180 ) ) ;
#25827=CARTESIAN_POINT ( 'NONE',  ( -6.542779104410481494, 20.88585256366161502, -1.500000000000002220 ) ) ;
#25828=CARTESIAN_POINT ( 'NONE',  ( -69.54933722304251376, -24.15620529776627734, 10.23563542870660825 ) ) ;
#25829=CARTESIAN_POINT ( 'NONE',  ( -27.12033265819623296, -24.75670803537512654, 2.403093704482753612 ) ) ;
#25830=CARTESIAN_POINT ( 'NONE',  ( -54.52287095715008292, -23.72747288104469732, -1.053458166803227680 ) ) ;
#25831=CARTESIAN_POINT ( 'NONE',  ( -58.61166247586906763, -23.48783264082476663, -1.443836473390093689 ) ) ;
#25832=ORIENTED_EDGE ( 'NONE', *, *, #100331, .T. ) ;
#25833=CARTESIAN_POINT ( 'NONE',  ( -14.48729221511043441, 14.40292172154154926, -1.500000000000002220 ) ) ;
#25835=ORIENTED_EDGE ( 'NONE', *, *, #41905, .T. ) ;
#25836=CARTESIAN_POINT ( 'NONE',  ( 5.527175565732886042, -22.34193536506064603, -1.500000000000002220 ) ) ;
#25838=ORIENTED_EDGE ( 'NONE', *, *, #72044, .F. ) ;
#25839=LINE ( 'NONE', #57810, #63960 ) ;
#25840=PLANE ( 'NONE',  #35234 ) ;
#25841=CARTESIAN_POINT ( 'NONE',  ( -122.5895376238167245, -24.66019654487200086, 8.947790411086115725 ) ) ;
#25842=CARTESIAN_POINT ( 'NONE',  ( -118.3655821056664905, -25.21790522177258609, 6.461928009673355788 ) ) ;
#25843=CARTESIAN_POINT ( 'NONE',  ( -20.23222619987061677, -6.887663580918623296, 11.49999999999999645 ) ) ;
#25844=VERTEX_POINT ( 'NONE', #54960 ) ;
#25845=EDGE_CURVE ( 'NONE', #33324, #27253, #62564, .T. ) ;
#25846=ORIENTED_EDGE ( 'NONE', *, *, #61370, .F. ) ;
#25847=CARTESIAN_POINT ( 'NONE',  ( 14.93699691249320693, 16.48547057857716425, -1.500000000000002220 ) ) ;
#25848=ADVANCED_FACE ( 'NONE', ( #71184 ), #86399, .T. ) ;
#25849=CARTESIAN_POINT ( 'NONE',  ( 0.1934390699377774303, 20.68474938276070318, 11.49999999999998934 ) ) ;
#25851=VERTEX_POINT ( 'NONE', #9267 ) ;
#25855=CARTESIAN_POINT ( 'NONE',  ( -127.5562042904833930, -24.64898659630529920, 1.056161002820838579 ) ) ;
#25857=EDGE_LOOP ( 'NONE', ( #68533, #19639, #88742, #67272 ) ) ;
#25859=B_SPLINE_CURVE_WITH_KNOTS ( 'NONE', 3,
 ( #27808, #28804, #20684, #28306 ),
 .UNSPECIFIED., .F., .F.,
 ( 4, 4 ),
 ( 0.000000000000000000, 9.999999999998206125E-05 ),
 .UNSPECIFIED. ) ;
#25860=CARTESIAN_POINT ( 'NONE',  ( -71.27267509207285912, -25.21912432202341492, 6.451068343402560856 ) ) ;
#25861=CARTESIAN_POINT ( 'NONE',  ( 2.299058169534009100, 20.76012671103276475, -1.500000000000002220 ) ) ;
#25863=CARTESIAN_POINT ( 'NONE',  ( 17.34737195785526609, 13.27887811287985187, 11.49999999999999645 ) ) ;
#25864=CARTESIAN_POINT ( 'NONE',  ( -73.63909330937920572, -23.96169478059713143, 10.65365249895718236 ) ) ;
#25865=DIRECTION ( 'NONE',  ( -3.773278334453079030E-23, 0.9999999999976377785, 2.173523156925979128E-06 ) ) ;
#25866=CARTESIAN_POINT ( 'NONE',  ( -21.16806448877717628, 7.570426553894726851, 11.49999999999998934 ) ) ;
#25867=AXIS2_PLACEMENT_3D ( 'NONE', #8150, #528, #31479 ) ;
#25868=CARTESIAN_POINT ( 'NONE',  ( -19.40224465947428456, -7.824916089261592766, 11.49999999999998934 ) ) ;
#25869=CARTESIAN_POINT ( 'NONE',  ( -38.55293158061942194, -23.96119346886880663, -0.6495511937831989213 ) ) ;
#25870=CARTESIAN_POINT ( 'NONE',  ( -52.58953762381673158, -24.66019654487199020, 8.947790411086131712 ) ) ;
#25871=CARTESIAN_POINT ( 'NONE',  ( -126.5228709571500616, -24.66019654487200441, 8.947790411086108620 ) ) ;
#25874=ORIENTED_EDGE ( 'NONE', *, *, #93165, .F. ) ;
#25876=ORIENTED_EDGE ( 'NONE', *, *, #52998, .T. ) ;
#25880=CARTESIAN_POINT ( 'NONE',  ( 21.20698605602738951, -2.876969938318672870, -1.500000000000002220 ) ) ;
#25881=CARTESIAN_POINT ( 'NONE',  ( -1.986123035288760885, 22.30159847666916662, 11.49999999999999645 ) ) ;
#25882=VERTEX_POINT ( 'NONE', #79280 ) ;
#25884=CARTESIAN_POINT ( 'NONE',  ( 0.4554788648648982474, -21.05657754196055009, -1.500000000000002220 ) ) ;
#25885=CARTESIAN_POINT ( 'NONE',  ( -30.51840328450298756, -23.78345446126201068, 10.97490056816818971 ) ) ;
#25886=CARTESIAN_POINT ( 'NONE',  ( 18.73470368118781693, 6.836574088118649861, -1.500000000000002220 ) ) ;
#25887=CARTESIAN_POINT ( 'NONE',  ( -50.48313689439709862, -24.73531770709094602, 8.716586749053508498 ) ) ;
#25889=CARTESIAN_POINT ( 'NONE',  ( 20.91424602935089894, 6.983905699820807556, -1.500000000000002220 ) ) ;
#25890=ORIENTED_EDGE ( 'NONE', *, *, #3414, .F. ) ;
#25891=CARTESIAN_POINT ( 'NONE',  ( -116.5196432029274973, -23.96119346886881729, -0.6495511937831834892 ) ) ;
#25892=PLANE ( 'NONE',  #61088 ) ;
#25893=CARTESIAN_POINT ( 'NONE',  ( -41.02425807142757463, -25.27956050905338259, 5.449277030247038134 ) ) ;
#25894=EDGE_CURVE ( 'NONE', #46787, #22811, #52853, .T. ) ;
#25895=CARTESIAN_POINT ( 'NONE',  ( -47.52287095715007581, -23.94994826722564696, -0.6494450866342728057 ) ) ;
#25897=LINE ( 'NONE', #17789, #35136 ) ;
#25898=CARTESIAN_POINT ( 'NONE',  ( -1.825377252022436281, -21.23478267787193730, -1.500000000000002220 ) ) ;
#25899=CARTESIAN_POINT ( 'NONE',  ( -97.52287095715006160, -24.64898659630367916, 1.056161002820829697 ) ) ;
#25900=DIRECTION ( 'NONE',  ( 0.000000000000000000, -0.9999999999976377785, -2.173523156925979128E-06 ) ) ;
#25902=CARTESIAN_POINT ( 'NONE',  ( -32.22287095715006444, -23.47596703998600276, 11.44779298504227683 ) ) ;
#25903=CARTESIAN_POINT ( 'NONE',  ( -107.6228709571500701, -29.50250243563736774, 8.947779886222136270 ) ) ;
#25904=CARTESIAN_POINT ( 'NONE',  ( 15.88279217892459094, 16.07415641707351384, -1.500000000000002220 ) ) ;
#25905=CARTESIAN_POINT ( 'NONE',  ( -81.52287095715006160, -24.64898659630367916, 1.056161002820826145 ) ) ;
#25906=ORIENTED_EDGE ( 'NONE', *, *, #24045, .F. ) ;
#25909=CARTESIAN_POINT ( 'NONE',  ( -11.90832679833862073, -15.64659449181510986, 11.49999999999999645 ) ) ;
#25911=CARTESIAN_POINT ( 'NONE',  ( -67.64073392607424751, -23.96119346886880308, -0.6495511937832114668 ) ) ;
#25915=CARTESIAN_POINT ( 'NONE',  ( -124.5563175255059605, -23.73791477778912551, 11.05961554403169878 ) ) ;
#25916=FACE_OUTER_BOUND ( 'NONE', #63578, .T. ) ;
#25917=CARTESIAN_POINT ( 'NONE',  ( -58.52287095715006160, -23.47596703998600631, 11.44779298504228926 ) ) ;
#25918=B_SPLINE_CURVE_WITH_KNOTS ( 'NONE', 3,
 ( #18976, #3281, #40325, #40818 ),
 .UNSPECIFIED., .F., .F.,
 ( 4, 4 ),
 ( 0.5401716478292172274, 0.5491780791013332053 ),
 .UNSPECIFIED. ) ;
#25920=CARTESIAN_POINT ( 'NONE',  ( -1.996473883165060581, 19.68112600131995293, 11.49999999999998934 ) ) ;
#25921=EDGE_LOOP ( 'NONE', ( #27960, #96041, #51431, #26064 ) ) ;
#25922=CARTESIAN_POINT ( 'NONE',  ( 3.569899647507075890, 19.86734082857295647, 11.49999999999999645 ) ) ;
#25927=CARTESIAN_POINT ( 'NONE',  ( -52.58953762381672448, -24.65952944569304250, 1.056160979905697239 ) ) ;
#25928=CARTESIAN_POINT ( 'NONE',  ( -65.55620429048339304, -23.48786465467240703, 11.44779295918254647 ) ) ;
#25931=AXIS2_PLACEMENT_3D ( 'NONE', #73764, #4759, #74267 ) ;
#25932=CARTESIAN_POINT ( 'NONE',  ( -62.52287095715006160, -23.48786465467241058, 11.44779295918254824 ) ) ;
#25933=CARTESIAN_POINT ( 'NONE',  ( -120.5895376238167245, -23.48786465467241769, 11.44779295918253759 ) ) ;
#25934=CARTESIAN_POINT ( 'NONE',  ( 19.36564117097816862, 5.170944958934900804, 11.49999999999998934 ) ) ;
#25935=CARTESIAN_POINT ( 'NONE',  ( -34.52287095715006160, -24.64898659630366851, 1.056161002820817485 ) ) ;
#25936=ORIENTED_EDGE ( 'NONE', *, *, #96604, .F. ) ;
#25937=ADVANCED_FACE ( 'NONE', ( #3678 ), #56972, .F. ) ;
#25940=CARTESIAN_POINT ( 'NONE',  ( -51.52287095715009002, -23.48783264082477018, -1.443836473390092578 ) ) ;
#25941=CARTESIAN_POINT ( 'NONE',  ( -35.52138534232717859, -24.92564183028978775, 1.928384488918258199 ) ) ;
#25942=CARTESIAN_POINT ( 'NONE',  ( -80.43221577628075636, -25.30553498687082481, 4.967019777649441359 ) ) ;
#25945=CARTESIAN_POINT ( 'NONE',  ( -103.5228709571501042, -23.48783264082477018, -1.443836473390087916 ) ) ;
#25950=CARTESIAN_POINT ( 'NONE',  ( 12.41260344771940360, 16.11316662856288318, -1.500000000000002220 ) ) ;
#25951=ORIENTED_EDGE ( 'NONE', *, *, #52994, .F. ) ;
#25952=EDGE_CURVE ( 'NONE', #47563, #65800, #97013, .T. ) ;
#25954=CARTESIAN_POINT ( 'NONE',  ( -127.5896351818574459, -24.35071581493543746, 9.817618358456011052 ) ) ;
#25955=ORIENTED_EDGE ( 'NONE', *, *, #79716, .T. ) ;
#25956=CARTESIAN_POINT ( 'NONE',  ( -59.64911270062432891, -23.73791477778911840, 11.05961554403171299 ) ) ;
#25957=CARTESIAN_POINT ( 'NONE',  ( -49.84148113843717454, -25.26264154704761111, 6.992077779497625656 ) ) ;
#25958=CARTESIAN_POINT ( 'NONE',  ( -30.47287095715006799, -24.99299043464974091, 2.200638162335478487 ) ) ;
#25959=CARTESIAN_POINT ( 'NONE',  ( 19.97935793590388442, -6.945280299276400449, 11.49999999999999645 ) ) ;
#25960=CARTESIAN_POINT ( 'NONE',  ( 21.88104185797606505, 3.448541436957560880, 11.49999999999998934 ) ) ;
#25961=EDGE_CURVE ( 'NONE', #46475, #80523, #89164, .T. ) ;
#25962=CARTESIAN_POINT ( 'NONE',  ( -4.563637348303267949, -20.04915943051449645, -1.500000000000002220 ) ) ;
#25963=ORIENTED_EDGE ( 'NONE', *, *, #50384, .F. ) ;
#25964=CARTESIAN_POINT ( 'NONE',  ( -41.58133722831164647, -24.51314013834315375, 0.6176544820404115121 ) ) ;
#25965=VERTEX_POINT ( 'NONE', #49864 ) ;
#25967=CARTESIAN_POINT ( 'NONE',  ( -54.59888152181910215, -23.96119346886879953, -0.6495511937832153526 ) ) ;
#25968=CARTESIAN_POINT ( 'NONE',  ( -110.6228709571500701, -24.92604778743018912, 8.074972756849355449 ) ) ;
#25971=VERTEX_POINT ( 'NONE', #28004 ) ;
#25972=CARTESIAN_POINT ( 'NONE',  ( -81.62287095715008434, -23.47596703998600631, 11.44779298504227860 ) ) ;
#25975=CARTESIAN_POINT ( 'NONE',  ( 7.914317726235799100, 19.11507755054979896, -1.500000000000002220 ) ) ;
#25977=CARTESIAN_POINT ( 'NONE',  ( 16.53012286974688294, -13.99140274789385252, 11.49999999999999645 ) ) ;
#25979=CARTESIAN_POINT ( 'NONE',  ( -69.55126625704998844, -25.16221347177320666, 3.076695569926833684 ) ) ;
#25980=CARTESIAN_POINT ( 'NONE',  ( -111.2965753446675450, -25.17176379221491800, 3.202224473218894030 ) ) ;
#25981=CARTESIAN_POINT ( 'NONE',  ( 0.2029947971921062799, -22.41465419638480228, 11.49999999999998934 ) ) ;
#25982=EDGE_CURVE ( 'NONE', #57364, #56711, #2001, .T. ) ;
#25985=ORIENTED_EDGE ( 'NONE', *, *, #216, .T. ) ;
#25987=CARTESIAN_POINT ( 'NONE',  ( -35.53214346113144728, -24.63419186844611630, 9.035850630976925757 ) ) ;
#25989=ORIENTED_EDGE ( 'NONE', *, *, #13634, .T. ) ;
#25991=CARTESIAN_POINT ( 'NONE',  ( -46.58712800869141546, -24.35071581493542325, 9.817618358456032368 ) ) ;
#25994=CARTESIAN_POINT ( 'NONE',  ( 20.00388196354723291, 7.160935007556333609, -1.500000000000002220 ) ) ;
#25996=CARTESIAN_POINT ( 'NONE',  ( -88.63497506943951976, -23.96119346886881019, -0.6495511937832099125 ) ) ;
#25997=CARTESIAN_POINT ( 'NONE',  ( 3.468383421097696928, -21.53508805063734854, 11.49999999999998934 ) ) ;
#25998=CARTESIAN_POINT ( 'NONE',  ( -103.5221972247327784, -23.48786465467241058, 11.44779295918254292 ) ) ;
#25999=CARTESIAN_POINT ( 'NONE',  ( -51.62287095715005592, -29.50247984919015209, -1.443849546365058689 ) ) ;
#26001=CARTESIAN_POINT ( 'NONE',  ( 17.34737195785526609, 13.27887811287985187, -1.500000000000002220 ) ) ;
#26003=ORIENTED_EDGE ( 'NONE', *, *, #96759, .T. ) ;
#26004=CARTESIAN_POINT ( 'NONE',  ( -89.62287095715004170, -24.64965695001468404, 8.947790433994180503 ) ) ;
#26005=CARTESIAN_POINT ( 'NONE',  ( -48.91945971812886995, -25.26337384518503271, 6.515678376904751268 ) ) ;
#26006=EDGE_LOOP ( 'NONE', ( #33712, #58550, #99546, #9330 ) ) ;
#26010=CARTESIAN_POINT ( 'NONE',  ( -128.5895376238167103, -23.47596703998600631, 11.44779298504227683 ) ) ;
#26013=CARTESIAN_POINT ( 'NONE',  ( 12.23393567461250697, 17.36540613969008007, -1.500000000000002220 ) ) ;
#26015=CARTESIAN_POINT ( 'NONE',  ( -30.59167141582165783, -24.92410949913933038, 1.600845668900849672 ) ) ;
#26017=CARTESIAN_POINT ( 'NONE',  ( -68.58036413909906059, -24.65952944569304606, 1.056160979905701236 ) ) ;
#26019=CARTESIAN_POINT ( 'NONE',  ( -7.106217341473486826, 18.08270997100935418, 11.49999999999998934 ) ) ;
#26020=EDGE_CURVE ( 'NONE', #68431, #76612, #42746, .T. ) ;
#26021=CARTESIAN_POINT ( 'NONE',  ( -93.62287095715005592, -29.50248528299804818, 1.056150453629040253 ) ) ;
#26022=ORIENTED_EDGE ( 'NONE', *, *, #70527, .F. ) ;
#26023=CARTESIAN_POINT ( 'NONE',  ( 6.966380261627926451, -18.21767524041069564, 11.49999999999999645 ) ) ;
#26028=CARTESIAN_POINT ( 'NONE',  ( -75.62287095715005592, -23.48783264082478084, -1.443836473390065489 ) ) ;
#26030=CARTESIAN_POINT ( 'NONE',  ( -81.23841534186585989, -25.03156017793848420, 7.364952925001797546 ) ) ;
#26031=CARTESIAN_POINT ( 'NONE',  ( -16.08770303010339831, 11.32657509950784736, 11.49999999999998934 ) ) ;
#26034=CARTESIAN_POINT ( 'NONE',  ( 21.72910700495702230, 7.846448622349001312, -1.500000000000002220 ) ) ;
#26035=ADVANCED_FACE ( 'NONE', ( #96016 ), #66096, .T. ) ;
#26038=CARTESIAN_POINT ( 'NONE',  ( -108.5228709571500616, -29.50250243563736774, 8.947779886222136270 ) ) ;
#26039=CARTESIAN_POINT ( 'NONE',  ( -51.52287095715008292, -23.47593901973090169, -1.443836447538997092 ) ) ;
#26041=CARTESIAN_POINT ( 'NONE',  ( -97.59657388994536120, -23.73791477778912196, 11.05961554403170410 ) ) ;
#26042=CARTESIAN_POINT ( 'NONE',  ( -78.92547529514705218, -25.27183487616304447, 3.712349674769177543 ) ) ;
#26044=CARTESIAN_POINT ( 'NONE',  ( -69.38261850605717029, -25.31201727726708128, 5.944601339124433004 ) ) ;
#26047=CARTESIAN_POINT ( 'NONE',  ( -1.345660788846553935, -19.86331345790170033, 11.49999999999998934 ) ) ;
#26048=CARTESIAN_POINT ( 'NONE',  ( -75.64171577028287174, -24.15602025860895807, 10.28564288303536678 ) ) ;
#26049=CARTESIAN_POINT ( 'NONE',  ( 2.793900936927258272, 19.68708943014846469, -1.500000000000002220 ) ) ;
#26050=ORIENTED_EDGE ( 'NONE', *, *, #67258, .T. ) ;
#26054=EDGE_CURVE ( 'NONE', #54341, #46190, #91463, .T. ) ;
#26055=CARTESIAN_POINT ( 'NONE',  ( -104.6228709571500985, -24.50321055353805377, 9.387540953477529371 ) ) ;
#26056=CARTESIAN_POINT ( 'NONE',  ( -29.52287095715007226, -23.87625476476128128, 10.65359472914277816 ) ) ;
#26057=CARTESIAN_POINT ( 'NONE',  ( -80.49261886157198376, -25.00182538069146787, 7.747789668545041586 ) ) ;
#26058=CARTESIAN_POINT ( 'NONE',  ( 0.4431998670617953717, 20.78131286043265646, 11.49999999999999645 ) ) ;
#26061=CARTESIAN_POINT ( 'NONE',  ( -51.08354598259256107, -25.21593214439643305, 3.527498281770244493 ) ) ;
#26063=CARTESIAN_POINT ( 'NONE',  ( -21.74551633039419585, 6.958787177381512201, 11.49999999999999645 ) ) ;
#26064=ORIENTED_EDGE ( 'NONE', *, *, #87184, .F. ) ;
#26065=CARTESIAN_POINT ( 'NONE',  ( -108.5895376238167387, -24.64965694238407679, 8.947790433994649462 ) ) ;
#26066=CARTESIAN_POINT ( 'NONE',  ( -84.62287095715008434, -23.47596703998600631, 11.44779298504227860 ) ) ;
#26068=CARTESIAN_POINT ( 'NONE',  ( -16.41926757845921614, -11.79510067912178606, -1.500000000000002220 ) ) ;
#26073=EDGE_LOOP ( 'NONE', ( #64954, #73440, #41813, #24269 ) ) ;
#26074=CARTESIAN_POINT ( 'NONE',  ( -70.62287095715008434, -24.82576562982391977, 8.398263435472967942 ) ) ;
#26077=CARTESIAN_POINT ( 'NONE',  ( 19.86090765050778728, -2.328952942160339212, -1.500000000000002220 ) ) ;
#26078=CARTESIAN_POINT ( 'NONE',  ( 7.117523389609132778, 19.69228268689324324, 11.49999999999999645 ) ) ;
#26079=VECTOR ( 'NONE', #25721, 1000.000000000000114 ) ;
#26080=CARTESIAN_POINT ( 'NONE',  ( -54.62287095715004170, -24.51387760970723662, 9.387446482453421837 ) ) ;
#26081=CARTESIAN_POINT ( 'NONE',  ( -93.52287095715006160, -24.51387760970725083, 9.387446482453398744 ) ) ;
#26082=CARTESIAN_POINT ( 'NONE',  ( 7.103389721457689099, 20.86620700561973862, -1.500000000000002220 ) ) ;
#26083=EDGE_CURVE ( 'NONE', #86142, #10167, #60468, .T. ) ;
#26084=CARTESIAN_POINT ( 'NONE',  ( -39.93582354980947002, -25.27806084964504407, 4.982375622346077115 ) ) ;
#26085=ORIENTED_EDGE ( 'NONE', *, *, #46920, .F. ) ;
#26086=CARTESIAN_POINT ( 'NONE',  ( -60.52287095715007581, -24.82558206586143612, 1.605769216559444379 ) ) ;
#26090=VERTEX_POINT ( 'NONE', #20875 ) ;
#26092=VERTEX_POINT ( 'NONE', #13261 ) ;
#26093=ORIENTED_EDGE ( 'NONE', *, *, #34767, .F. ) ;
#26095=CARTESIAN_POINT ( 'NONE',  ( -100.7878122855614293, -25.27404639244512907, 2.873139757414048479 ) ) ;
#26096=CARTESIAN_POINT ( 'NONE',  ( -110.5228709571500616, -29.50249982740957577, 7.747779886224967605 ) ) ;
#26097=CARTESIAN_POINT ( 'NONE',  ( -9.284664653622879626, 18.31210316397345395, -1.500000000000002220 ) ) ;
#26098=B_SPLINE_CURVE_WITH_KNOTS ( 'NONE', 3,
 ( #74383, #57190, #26716, #95728, #57677, #80498 ),
 .UNSPECIFIED., .F., .F.,
 ( 4, 2, 4 ),
 ( 0.000000000000000000, 0.001380901958385393966, 0.002761803916770787931 ),
 .UNSPECIFIED. ) ;
#26100=ORIENTED_EDGE ( 'NONE', *, *, #39779, .F. ) ;
#26102=CARTESIAN_POINT ( 'NONE',  ( -102.6228709571500559, -24.65952944569304606, 1.056160979905702124 ) ) ;
#26104=CARTESIAN_POINT ( 'NONE',  ( -7.907391756136429528, -20.87048397725295956, -1.500000000000002220 ) ) ;
#26106=CARTESIAN_POINT ( 'NONE',  ( -0.1490770655183801252, -21.12008023607309681, -1.443836447538997758 ) ) ;
#26107=CARTESIAN_POINT ( 'NONE',  ( -113.5228709571500616, -23.47596703998600631, 11.44779298504228038 ) ) ;
#26108=EDGE_LOOP ( 'NONE', ( #9595, #82987, #13183, #28303 ) ) ;
#26109=EDGE_CURVE ( 'NONE', #63576, #73782, #22856, .T. ) ;
#26110=CARTESIAN_POINT ( 'NONE',  ( -32.62287095715005592, -24.33927499327854704, 9.819080762295817166 ) ) ;
#26112=CARTESIAN_POINT ( 'NONE',  ( -9.832896139050584239, -18.40278743011522877, 11.49999999999998934 ) ) ;
#26116=EDGE_LOOP ( 'NONE', ( #80142, #88906, #50717, #67035 ) ) ;
#26118=ADVANCED_FACE ( 'NONE', ( #36607 ), #14255, .T. ) ;
#26119=CARTESIAN_POINT ( 'NONE',  ( 2.700122536338566359, 20.86363338933649558, -1.500000000000002220 ) ) ;
#26121=CARTESIAN_POINT ( 'NONE',  ( -114.6228709571500275, -24.33927499327855060, 9.819080762295804732 ) ) ;
#26123=CARTESIAN_POINT ( 'NONE',  ( -120.6241460807069075, -24.83644354573579349, 8.397322867130096569 ) ) ;
#26124=CARTESIAN_POINT ( 'NONE',  ( -101.2262178754702120, -25.25419513428566987, 7.375460839105605793 ) ) ;
#26125=CARTESIAN_POINT ( 'NONE',  ( -36.58953762381673158, -24.65952944569304250, 1.056160979905695019 ) ) ;
#26126=CARTESIAN_POINT ( 'NONE',  ( -10.04279811845843007, 19.21892966915218892, -1.500000000000002220 ) ) ;
#26128=CARTESIAN_POINT ( 'NONE',  ( -21.31523168734759466, -6.469442287714795015, 11.49999999999999645 ) ) ;
#26130=CARTESIAN_POINT ( 'NONE',  ( -72.62287095715004170, -23.96177878511307568, 10.65340807706330217 ) ) ;
#26131=DIRECTION ( 'NONE',  ( 3.773278334444167608E-23, -1.000000000000000000, 0.000000000000000000 ) ) ;
#26132=CARTESIAN_POINT ( 'NONE',  ( -75.52287095715007581, -29.50250786944525672, 11.44777988621623521 ) ) ;
#26133=EDGE_LOOP ( 'NONE', ( #12229, #78219, #31940, #23221 ) ) ;
#26135=ORIENTED_EDGE ( 'NONE', *, *, #9917, .F. ) ;
#26136=ORIENTED_EDGE ( 'NONE', *, *, #5582, .F. ) ;
#26137=CARTESIAN_POINT ( 'NONE',  ( -86.52287095715006160, -24.64965694238575011, 8.947790433994196491 ) ) ;
#26138=VECTOR ( 'NONE', #71983, 1000.000000000000114 ) ;
#26142=CARTESIAN_POINT ( 'NONE',  ( -130.5728709571500588, -24.25872324547561831, -0.2236092734016485173 ) ) ;
#26143=CARTESIAN_POINT ( 'NONE',  ( 8.126467401150291536, 20.86698325809501497, -1.500000000000002220 ) ) ;
#26144=B_SPLINE_CURVE_WITH_KNOTS ( 'NONE', 3,
 ( #90851, #22816, #38059, #92839, #31450, #14212 ),
 .UNSPECIFIED., .F., .F.,
 ( 4, 2, 4 ),
 ( 0.000000000000000000, 0.001380901958385390930, 0.002761803916770781860 ),
 .UNSPECIFIED. ) ;
#26147=LINE ( 'NONE', #72837, #41753 ) ;
#26148=CARTESIAN_POINT ( 'NONE',  ( -101.5985644930808007, -23.48786465467240703, 11.44779295918254114 ) ) ;
#26149=CARTESIAN_POINT ( 'NONE',  ( -61.52287095715007581, -24.33927499327854349, 9.819080762295813614 ) ) ;
#26151=CARTESIAN_POINT ( 'NONE',  ( -30.60521428952115741, -24.47917135695840685, 9.440663514584130667 ) ) ;
#26153=CARTESIAN_POINT ( 'NONE',  ( -16.94305004876727239, 9.801747318927828800, 11.49999999999998934 ) ) ;
#26154=CARTESIAN_POINT ( 'NONE',  ( -49.56549000277595241, -25.29186519241541831, 4.241630633777523585 ) ) ;
#26156=ORIENTED_EDGE ( 'NONE', *, *, #24334, .F. ) ;
#26157=CARTESIAN_POINT ( 'NONE',  ( -20.54356019850136050, 6.435454313062578535, 11.49999999999998934 ) ) ;
#26159=CARTESIAN_POINT ( 'NONE',  ( -71.14319566529317740, -25.12219058256228266, 6.703707996014909298 ) ) ;
#26160=CARTESIAN_POINT ( 'NONE',  ( -100.4381051993576364, -25.12049752546738191, 2.832404795212222215 ) ) ;
#26162=CARTESIAN_POINT ( 'NONE',  ( 19.00551534866085746, 12.86435971046890359, -1.500000000000002220 ) ) ;
#26166=CARTESIAN_POINT ( 'NONE',  ( -49.59948389210610742, -23.96119346886879953, -0.6495511937832114668 ) ) ;
#26167=CARTESIAN_POINT ( 'NONE',  ( 3.315226082619958881, 19.80964767386612380, 11.49999999999999645 ) ) ;
#26169=CARTESIAN_POINT ( 'NONE',  ( -31.52287095715007581, -23.73907113217667231, -1.053371485781312344 ) ) ;
#26170=EDGE_CURVE ( 'NONE', #11739, #64035, #45494, .T. ) ;
#26171=DIRECTION ( 'NONE',  ( 0.000000000000000000, 0.9999999999976377785, 2.173523156925979975E-06 ) ) ;
#26172=CARTESIAN_POINT ( 'NONE',  ( -65.62287095715008434, -24.62226745350439217, 0.9660975649728189563 ) ) ;
#26174=CARTESIAN_POINT ( 'NONE',  ( 1.158388978951967463, 19.79969207489630634, 11.49999999999998934 ) ) ;
#26175=EDGE_CURVE ( 'NONE', #51553, #79008, #83027, .T. ) ;
#26176=CARTESIAN_POINT ( 'NONE',  ( -90.62287095715009855, -24.15516710230295061, 10.28746687063727450 ) ) ;
#26177=CARTESIAN_POINT ( 'NONE',  ( -19.50520112914412252, -2.896358124273927359, -1.500000000000002220 ) ) ;
#26178=ADVANCED_FACE ( 'NONE', ( #75653 ), #29484, .F. ) ;
#26179=CARTESIAN_POINT ( 'NONE',  ( -89.49044894935767047, -25.12049752546738191, 2.832404795212222659 ) ) ;
#26180=EDGE_CURVE ( 'NONE', #66017, #59957, #6653, .T. ) ;
#26186=CARTESIAN_POINT ( 'NONE',  ( -16.41017380093149214, -12.48182641202616416, 11.49999999999999645 ) ) ;
#26189=CARTESIAN_POINT ( 'NONE',  ( 18.14931799402153345, 13.46472642042223633, 11.49999999999999645 ) ) ;
#26191=ORIENTED_EDGE ( 'NONE', *, *, #63336, .T. ) ;
#26192=CARTESIAN_POINT ( 'NONE',  ( -126.5228709571500616, -23.47593901973090524, -1.443836447538996204 ) ) ;
#26193=CARTESIAN_POINT ( 'NONE',  ( -51.15093573314597819, -25.30062286728702148, 4.392258012681271140 ) ) ;
#26196=CARTESIAN_POINT ( 'NONE',  ( -27.40807623642065494, -24.61460109215988723, 8.230616185672861462 ) ) ;
#26198=B_SPLINE_CURVE_WITH_KNOTS ( 'NONE', 3,
 ( #11612, #81133, #42089, #12109 ),
 .UNSPECIFIED., .F., .F.,
 ( 4, 4 ),
 ( 0.000000000000000000, 1.000000000000000000 ),
 .UNSPECIFIED. ) ;
#26200=EDGE_CURVE ( 'NONE', #99597, #88647, #81780, .T. ) ;
#26201=CARTESIAN_POINT ( 'NONE',  ( 16.03631736716203449, -16.64276770305488284, 11.49999999999999645 ) ) ;
#26202=CARTESIAN_POINT ( 'NONE',  ( 13.94817355369617751, 18.09530419158152625, -1.500000000000002220 ) ) ;
#26204=CARTESIAN_POINT ( 'NONE',  ( -106.6228709571501412, -24.35013146730204170, 9.818937971375106599 ) ) ;
#26205=CARTESIAN_POINT ( 'NONE',  ( -82.62936503442081460, -24.35071581493543036, 9.817618358456032368 ) ) ;
#26206=CARTESIAN_POINT ( 'NONE',  ( -21.13723655771239152, -7.639886366525781014, 11.49999999999999645 ) ) ;
#26210=CARTESIAN_POINT ( 'NONE',  ( 1.410849576418898632, -21.91845101833037290, 11.49999999999998934 ) ) ;
#26213=CARTESIAN_POINT ( 'NONE',  ( -111.6258027458890751, -24.34968618360933945, 0.1864209137778883862 ) ) ;
#26214=CARTESIAN_POINT ( 'NONE',  ( -70.34543693012690824, -25.03284467579916495, 7.563174216508125269 ) ) ;
#26216=CARTESIAN_POINT ( 'NONE',  ( -48.54704611537135150, -24.15620529776628089, 10.23563542870660470 ) ) ;
#26219=CARTESIAN_POINT ( 'NONE',  ( -88.52287095715007581, -23.72747288104470087, -1.053458166803225460 ) ) ;
#26220=CARTESIAN_POINT ( 'NONE',  ( -7.444040098415714013, -19.11467064512029879, 11.49999999999998934 ) ) ;
#26222=VERTEX_POINT ( 'NONE', #9666 ) ;
#26223=ORIENTED_EDGE ( 'NONE', *, *, #49097, .F. ) ;
#26224=CARTESIAN_POINT ( 'NONE',  ( -50.11237177578891533, -25.31359240361684471, 5.223018419632965426 ) ) ;
#26225=CARTESIAN_POINT ( 'NONE',  ( 1.702247502073919394, 23.03039350466679025, 11.49999999999998934 ) ) ;
#26227=CARTESIAN_POINT ( 'NONE',  ( -14.79517943714664518, -13.99575967537150412, -1.500000000000002220 ) ) ;
#26230=CARTESIAN_POINT ( 'NONE',  ( -29.47547545905215927, -24.57318954944668832, 8.947790440257527678 ) ) ;
#26231=EDGE_CURVE ( 'NONE', #66719, #80383, #23728, .T. ) ;
#26233=CARTESIAN_POINT ( 'NONE',  ( -101.5292613482009898, -25.24695879370139906, 6.294269473182250607 ) ) ;
#26234=DIRECTION ( 'NONE',  ( 0.000000000000000000, -2.173523156925980399E-06, 0.9999999999976378895 ) ) ;
#26235=ORIENTED_EDGE ( 'NONE', *, *, #57251, .F. ) ;
#26236=CARTESIAN_POINT ( 'NONE',  ( -27.89567495842467082, -25.21531660661593222, 2.285878875735976479 ) ) ;
#26237=CARTESIAN_POINT ( 'NONE',  ( -49.19182681462018536, -25.26385729957443615, 4.415198428280462828 ) ) ;
#26240=CARTESIAN_POINT ( 'NONE',  ( -12.26507114386991226, -16.75673120704366426, 11.49999999999998934 ) ) ;
#26241=EDGE_CURVE ( 'NONE', #80639, #17917, #88973, .T. ) ;
#26242=ORIENTED_EDGE ( 'NONE', *, *, #40556, .F. ) ;
#26243=CARTESIAN_POINT ( 'NONE',  ( -102.6228709571500275, -23.48783264082478794, -1.443836473390062158 ) ) ;
#26245=B_SPLINE_CURVE_WITH_KNOTS ( 'NONE', 3,
 ( #60539, #91454, #84344, #52918 ),
 .UNSPECIFIED., .F., .F.,
 ( 4, 4 ),
 ( 0.6809862756305058440, 0.6899927069026217108 ),
 .UNSPECIFIED. ) ;
#26247=CARTESIAN_POINT ( 'NONE',  ( -51.93149462243456327, -25.24900417239232908, 6.174051150523328424 ) ) ;
#26248=ORIENTED_EDGE ( 'NONE', *, *, #44414, .F. ) ;
#26250=CARTESIAN_POINT ( 'NONE',  ( -88.58953762381671027, -24.65952944569304606, 1.056160979905700570 ) ) ;
#26251=CARTESIAN_POINT ( 'NONE',  ( -68.62287095715005592, -24.51387760970723662, 9.387446482453425389 ) ) ;
#26254=CARTESIAN_POINT ( 'NONE',  ( 13.62230711432095553, -17.35066874027886286, 11.49999999999999645 ) ) ;
#26256=CARTESIAN_POINT ( 'NONE',  ( -49.21454750704995007, -25.13877828889947352, 7.069183601642414772 ) ) ;
#26257=CARTESIAN_POINT ( 'NONE',  ( -21.70561270324154179, 6.225854807558039994, -1.500000000000002220 ) ) ;
#26259=ORIENTED_EDGE ( 'NONE', *, *, #62982, .F. ) ;
#26261=CARTESIAN_POINT ( 'NONE',  ( -93.62287095715005592, -23.47593901973091235, -1.443836447539002865 ) ) ;
#26262=B_SPLINE_CURVE_WITH_KNOTS ( 'NONE', 3,
 ( #25112, #49481, #26125, #8396 ),
 .UNSPECIFIED., .F., .F.,
 ( 4, 4 ),
 ( 0.000000000000000000, 9.999999999999592548E-05 ),
 .UNSPECIFIED. ) ;
#26264=CARTESIAN_POINT ( 'NONE',  ( -100.6228709571500559, -23.48783264082478794, -1.443836473390061936 ) ) ;
#26265=ORIENTED_EDGE ( 'NONE', *, *, #80711, .T. ) ;
#26266=CARTESIAN_POINT ( 'NONE',  ( 7.804836024166685426, 19.70032748343534834, 11.49999999999998934 ) ) ;
#26267=CARTESIAN_POINT ( 'NONE',  ( -78.94388818075310610, -25.27791636280661791, 6.014208090771517412 ) ) ;
#26268=CARTESIAN_POINT ( 'NONE',  ( -125.6228709571499991, -24.14321612903113135, -0.2833117244521720091 ) ) ;
#26270=CARTESIAN_POINT ( 'NONE',  ( -21.66996937300057269, -4.939502015459471096, -1.500000000000002220 ) ) ;
#26271=CARTESIAN_POINT ( 'NONE',  ( -74.62287095715004170, -23.72773821059536559, 11.05748984161097681 ) ) ;
#26272=B_SPLINE_CURVE_WITH_KNOTS ( 'NONE', 3,
 ( #453, #31408, #1471, #1973, #47145, #87195, #77064, #78062 ),
 .UNSPECIFIED., .F., .F.,
 ( 4, 2, 2, 4 ),
 ( -0.001240355328177008198, -0.0002398155169400597621, 0.0007607242942968886739, 0.002761803916770776655 ),
 .UNSPECIFIED. ) ;
#26276=CARTESIAN_POINT ( 'NONE',  ( -36.57552185154370505, -24.66019654487199730, 8.947790411086113949 ) ) ;
#26277=CARTESIAN_POINT ( 'NONE',  ( -58.62287095715004881, -29.50250786944525672, 11.44777988621623876 ) ) ;
#26278=CARTESIAN_POINT ( 'NONE',  ( -8.384790838521158918, 17.58144419890746235, -1.500000000000002220 ) ) ;
#26279=CARTESIAN_POINT ( 'NONE',  ( 21.40653236543258231, -1.377805879665675803, -1.500000000000002220 ) ) ;
#26282=B_SPLINE_CURVE_WITH_KNOTS ( 'NONE', 3,
 ( #89194, #3962, #57755, #3469, #35415, #18178 ),
 .UNSPECIFIED., .F., .F.,
 ( 4, 2, 4 ),
 ( 0.000000000000000000, 0.001380764517854759978, 0.002761529035709519957 ),
 .UNSPECIFIED. ) ;
#26285=CARTESIAN_POINT ( 'NONE',  ( -57.92287095715005307, -23.47593901973090169, -1.443836447538997758 ) ) ;
#26286=CARTESIAN_POINT ( 'NONE',  ( 10.71911242904675987, 20.06137936439360203, -1.500000000000002220 ) ) ;
#26289=CARTESIAN_POINT ( 'NONE',  ( -102.5127816447745062, -24.34968618360934656, 0.1864209137778959358 ) ) ;
#26290=DIRECTION ( 'NONE',  ( -1.000000000000000000, -3.773278334444167608E-23, -8.201307833595939069E-29 ) ) ;
#26291=CARTESIAN_POINT ( 'NONE',  ( 0.1862606309321278575, -19.90735222434816976, 11.49999999999999645 ) ) ;
#26292=CARTESIAN_POINT ( 'NONE',  ( -104.5511935059157480, -24.34968618360934300, 0.1864209137778872205 ) ) ;
#26294=EDGE_CURVE ( 'NONE', #55826, #52307, #76904, .T. ) ;
#26295=CARTESIAN_POINT ( 'NONE',  ( -39.49143307742559017, -24.35071581493542681, 9.817618358456035921 ) ) ;
#26296=CARTESIAN_POINT ( 'NONE',  ( -48.61470971034470523, -23.48783264082477729, -1.443836473390069486 ) ) ;
#26300=EDGE_CURVE ( 'NONE', #18231, #71801, #78168, .T. ) ;
#26301=CARTESIAN_POINT ( 'NONE',  ( 12.10466045530642631, 18.00204671274030233, -1.500000000000002220 ) ) ;
#26302=CARTESIAN_POINT ( 'NONE',  ( -56.60508433514527837, -23.73791477778912196, 11.05961554403170766 ) ) ;
#26303=CARTESIAN_POINT ( 'NONE',  ( -19.34354882100874562, 2.624169249526263403, -1.500000000000002220 ) ) ;
#26304=ADVANCED_FACE ( 'NONE', ( #94629 ), #33737, .F. ) ;
#26305=CARTESIAN_POINT ( 'NONE',  ( -55.50247564293582059, -24.15602025860896518, 10.28564288303535257 ) ) ;
#26311=CARTESIAN_POINT ( 'NONE',  ( -1.999887071766271784, 20.33596237858139233, 11.49999999999999645 ) ) ;
#26313=CARTESIAN_POINT ( 'NONE',  ( -118.6228709571499564, -24.51283580621365132, 0.6167428607019855846 ) ) ;
#26315=CARTESIAN_POINT ( 'NONE',  ( -55.62287095715006302, -23.48786465467240703, 11.44779295918255180 ) ) ;
#26317=CARTESIAN_POINT ( 'NONE',  ( -39.22484595018107711, -25.31628611224346770, 4.963672948320522416 ) ) ;
#26320=LINE ( 'NONE', #12074, #50026 ) ;
#26322=CARTESIAN_POINT ( 'NONE',  ( -42.55620429048338593, -24.65952944569303895, 1.056160979905692576 ) ) ;
#26323=CARTESIAN_POINT ( 'NONE',  ( 14.22603995551189371, 18.00578905361294346, 11.49999999999999645 ) ) ;
#26324=CARTESIAN_POINT ( 'NONE',  ( 21.64774270073068863, 7.000884456547583845, 11.49999999999998934 ) ) ;
#26326=B_SPLINE_SURFACE_WITH_KNOTS ( 'NONE', 3, 3, ( 
 ( #43979, #29243, #27755, #58705 ),
 ( #60216, #19133, #81044, #3934 ),
 ( #65849, #34871, #27265, #4923 ),
 ( #96765, #28754, #89158, #50596 ),
 ( #81551, #74909, #51098, #42993 ),
 ( #73933, #4431, #5414, #35379 ),
 ( #82043, #59211, #35866, #12522 ),
 ( #90155, #36367, #67324, #20630 ),
 ( #44988, #61712, #85022, #62211 ),
 ( #14513, #23113, #92634, #54101 ) ),
 .UNSPECIFIED., .F., .F., .F.,
 ( 4, 3, 3, 4 ),
 ( 4, 4 ),
 ( 0.7022005934544806038, 0.7765311282028792839, 0.8508616629512779639, 0.9995227324480753239 ),
 ( 0.1495120405554173637, 0.1506138728599011600 ),
 .UNSPECIFIED. ) ;
#26327=CARTESIAN_POINT ( 'NONE',  ( -80.52287095715006160, -29.50249982740957577, 7.747779886224967605 ) ) ;
#26328=CARTESIAN_POINT ( 'NONE',  ( -90.54141678234942958, -24.92564183028978775, 1.928384488918253092 ) ) ;
#26331=CARTESIAN_POINT ( 'NONE',  ( -16.30586240431254197, 14.59307310709210626, -1.500000000000002220 ) ) ;
#26332=CARTESIAN_POINT ( 'NONE',  ( -69.50621745294765219, -24.15620529776627734, 10.23563542870660825 ) ) ;
#26334=CARTESIAN_POINT ( 'NONE',  ( -48.89798248884767418, -25.28421271704163686, 5.878056207824126744 ) ) ;
#26336=CARTESIAN_POINT ( 'NONE',  ( -58.62775217774146341, -24.51314013834315020, 0.6176544820404091807 ) ) ;
#26339=CARTESIAN_POINT ( 'NONE',  ( -5.688044216684545518, -19.60349290560521140, 11.49999999999998934 ) ) ;
#26342=CARTESIAN_POINT ( 'NONE',  ( -9.967090755842360039, -20.75144515299163217, -1.500000000000002220 ) ) ;
#26343=CARTESIAN_POINT ( 'NONE',  ( -103.5228709571500758, -29.50250243563736774, 8.947779886222138046 ) ) ;
#26344=ORIENTED_EDGE ( 'NONE', *, *, #7999, .F. ) ;
#26346=CARTESIAN_POINT ( 'NONE',  ( -50.52287095715006160, -23.47593901973090169, -1.443836447538997092 ) ) ;
#26349=CARTESIAN_POINT ( 'NONE',  ( 21.39645853268639186, 0.3907444525687319703, 11.49999999999999645 ) ) ;
#26352=ORIENTED_EDGE ( 'NONE', *, *, #99941, .T. ) ;
#26353=CARTESIAN_POINT ( 'NONE',  ( -22.15176777451872425, 1.842445310382735624, 11.49999999999998934 ) ) ;
#26354=CARTESIAN_POINT ( 'NONE',  ( 3.345817365282868217, 20.41450801592841557, 11.49999999999998934 ) ) ;
#26356=ORIENTED_EDGE ( 'NONE', *, *, #90669, .F. ) ;
#26357=DIRECTION ( 'NONE',  ( -0.000000000000000000, 2.173523156925979552E-06, -0.9999999999976378895 ) ) ;
#26359=CARTESIAN_POINT ( 'NONE',  ( -70.79206301948316593, -25.20650855361216713, 6.812664954086296021 ) ) ;
#26361=PLANE ( 'NONE',  #64032 ) ;
#26362=B_SPLINE_CURVE_WITH_KNOTS ( 'NONE', 3,
 ( #29314, #44049, #67900, #45058 ),
 .UNSPECIFIED., .F., .F.,
 ( 4, 4 ),
 ( 0.000000000000000000, 0.0001000000000000167422 ),
 .UNSPECIFIED. ) ;
#26365=CARTESIAN_POINT ( 'NONE',  ( -2.496121100066326814, 20.73550571027955769, -1.500000000000002220 ) ) ;
#26366=CARTESIAN_POINT ( 'NONE',  ( 21.76694381678408519, 2.417257996116004115, 11.49999999999999645 ) ) ;
#26367=CARTESIAN_POINT ( 'NONE',  ( -106.6228709571500559, -24.65952944569304606, 1.056160979905703012 ) ) ;
#26369=CARTESIAN_POINT ( 'NONE',  ( 19.77564376705174709, 10.73071584254150856, 11.49999999999998934 ) ) ;
#26370=CARTESIAN_POINT ( 'NONE',  ( 7.117523389609132778, 19.69228268689324324, 11.49999999999998934 ) ) ;
#26371=CARTESIAN_POINT ( 'NONE',  ( -38.58105435577196118, -24.51314013834316086, 0.6176544820404135105 ) ) ;
#26377=VERTEX_POINT ( 'NONE', #80408 ) ;
#26379=B_SPLINE_CURVE_WITH_KNOTS ( 'NONE', 3,
 ( #7940, #25162, #38890, #24164 ),
 .UNSPECIFIED., .F., .F.,
 ( 4, 4 ),
 ( 0.000000000000000000, 9.999999999998897304E-05 ),
 .UNSPECIFIED. ) ;
#26380=CARTESIAN_POINT ( 'NONE',  ( -52.53220978181458634, -24.65952944569304606, 1.056160979905696351 ) ) ;
#26381=ORIENTED_EDGE ( 'NONE', *, *, #73053, .T. ) ;
#26382=CARTESIAN_POINT ( 'NONE',  ( 20.74164082462262471, 5.259929546262127609, -1.500000000000002220 ) ) ;
#26385=CARTESIAN_POINT ( 'NONE',  ( -26.11711738945389172, -24.95252434176281753, 5.477325856322839748 ) ) ;
#26386=CARTESIAN_POINT ( 'NONE',  ( -11.11193726737652199, 17.91617163517716804, -1.500000000000002220 ) ) ;
#26387=CARTESIAN_POINT ( 'NONE',  ( -61.62287095715004881, -23.47593901973091235, -1.443836447539007972 ) ) ;
#26389=CARTESIAN_POINT ( 'NONE',  ( -43.55620429048339304, -23.47596703998600276, 11.44779298504227505 ) ) ;
#26391=CARTESIAN_POINT ( 'NONE',  ( -129.5220745341863733, -23.96169478059714208, 10.65365249895717348 ) ) ;
#26392=CARTESIAN_POINT ( 'NONE',  ( -0.5447568859041533873, -22.05808898580190558, -1.500000000000002220 ) ) ;
#26393=AXIS2_PLACEMENT_3D ( 'NONE', #47103, #36595, #98984 ) ;
#26394=ORIENTED_EDGE ( 'NONE', *, *, #92724, .T. ) ;
#26395=CARTESIAN_POINT ( 'NONE',  ( -65.55175419035504092, -24.15602025860896518, 10.28564288303534724 ) ) ;
#26396=PLANE ( 'NONE',  #38398 ) ;
#26397=CARTESIAN_POINT ( 'NONE',  ( -41.25901049487872996, -25.31624695023827698, 5.328837378496615429 ) ) ;
#26399=CARTESIAN_POINT ( 'NONE',  ( -29.84429507560729178, -25.08342498570734591, 2.662461283694066427 ) ) ;
#26400=DIRECTION ( 'NONE',  ( 0.000000000000000000, -0.9999999999976377785, -2.173523156925979975E-06 ) ) ;
#26401=DIRECTION ( 'NONE',  ( 0.000000000000000000, -0.9999999999976377785, -2.173523156925979128E-06 ) ) ;
#26402=CARTESIAN_POINT ( 'NONE',  ( 13.79380260783658407, 16.28676726024703214, 11.49999999999998934 ) ) ;
#26403=CARTESIAN_POINT ( 'NONE',  ( -91.92287095715005307, -23.47596703998600631, 11.44779298504227860 ) ) ;
#26404=CARTESIAN_POINT ( 'NONE',  ( -49.88863945552024148, -25.20650842489795451, 6.812665538484691474 ) ) ;
#26405=CARTESIAN_POINT ( 'NONE',  ( -64.54379277406458471, -24.35071581493543391, 9.817618358456023486 ) ) ;
#26407=CARTESIAN_POINT ( 'NONE',  ( 4.940617368476682536, -22.01678987175928981, -1.500000000000002220 ) ) ;
#26409=B_SPLINE_SURFACE_WITH_KNOTS ( 'NONE', 3, 3, ( 
 ( #33633, #9278, #49371, #64105 ),
 ( #87919, #95026, #86411, #32120 ),
 ( #40243, #56982, #18402, #63092 ),
 ( #86909, #64613, #78284, #65107 ),
 ( #95527, #24505, #56489, #71195 ),
 ( #3198, #87410, #9788, #63598 ),
 ( #94521, #25002, #40739, #96027 ) ),
 .UNSPECIFIED., .F., .F., .F.,
 ( 4, 3, 4 ),
 ( 4, 4 ),
 ( 0.0004766839783839066499, 0.1029713700210905941, 0.2054660560637972810 ),
 ( 0.4796160033653972810, 0.4808500218641223456 ),
 .UNSPECIFIED. ) ;
#26410=CARTESIAN_POINT ( 'NONE',  ( -54.52287095715006870, -23.48786465467240347, 11.44779295918255002 ) ) ;
#26411=EDGE_LOOP ( 'NONE', ( #42995, #87645, #53924, #2923 ) ) ;
#26413=CARTESIAN_POINT ( 'NONE',  ( -31.58037117919289116, -24.51419770103156637, 9.386484678747187615 ) ) ;
#26414=CARTESIAN_POINT ( 'NONE',  ( -5.084378373094740944, 19.06436389234985285, 11.49999999999999645 ) ) ;
#26417=CARTESIAN_POINT ( 'NONE',  ( -67.55389679207142706, -23.96119346886879953, -0.6495511937832114668 ) ) ;
#26420=CARTESIAN_POINT ( 'NONE',  ( -127.4728709571500360, -25.21147115331108779, 5.000950862241218431 ) ) ;
#26422=EDGE_CURVE ( 'NONE', #47994, #56546, #48473, .T. ) ;
#26424=B_SPLINE_CURVE_WITH_KNOTS ( 'NONE', 3,
 ( #99327, #16455, #83602, #70258, #37444, #52668 ),
 .UNSPECIFIED., .F., .F.,
 ( 4, 2, 4 ),
 ( 0.000000000000000000, 0.001380901958385388545, 0.002761803916770777089 ),
 .UNSPECIFIED. ) ;
#26425=CARTESIAN_POINT ( 'NONE',  ( -21.57561264457377348, 0.06291308125064201673, 11.49999999999998934 ) ) ;
#26426=CARTESIAN_POINT ( 'NONE',  ( -88.62287095715004170, -23.47593901973091235, -1.443836447539002865 ) ) ;
#26427=CARTESIAN_POINT ( 'NONE',  ( -32.66693570750084774, -24.97155988971761431, 2.105726520353297548 ) ) ;
#26430=CARTESIAN_POINT ( 'NONE',  ( -81.57174390479045201, -25.13765173071444536, 7.079220311505046048 ) ) ;
#26431=CARTESIAN_POINT ( 'NONE',  ( -11.78406182805296254, 15.88391379356440503, -1.500000000000002220 ) ) ;
#26432=ORIENTED_EDGE ( 'NONE', *, *, #47546, .T. ) ;
#26433=B_SPLINE_CURVE_WITH_KNOTS ( 'NONE', 3,
 ( #29060, #90961, #20942, #53412, #82843, #84337 ),
 .UNSPECIFIED., .F., .F.,
 ( 4, 2, 4 ),
 ( 1.570755371634170283E-05, 0.001396183895866089705, 0.002776660238015837747 ),
 .UNSPECIFIED. ) ;
#26434=VECTOR ( 'NONE', #63245, 1000.000000000000227 ) ;
#26436=CARTESIAN_POINT ( 'NONE',  ( 17.43904876784772284, 10.37648870149486413, 11.49999999999999645 ) ) ;
#26441=CARTESIAN_POINT ( 'NONE',  ( -107.5228709571500758, -29.50250243563736774, 8.947779886222136270 ) ) ;
#26442=CARTESIAN_POINT ( 'NONE',  ( -51.48648995077594748, -25.27191416516480871, 5.909279887552581378 ) ) ;
#26445=CARTESIAN_POINT ( 'NONE',  ( -89.62287095715004170, -29.50248528299804818, 1.056150453629040253 ) ) ;
#26446=CARTESIAN_POINT ( 'NONE',  ( -5.935188749463110369, 19.13178230186815298, 11.49999999999998934 ) ) ;
#26447=EDGE_CURVE ( 'NONE', #62297, #12467, #12752, .T. ) ;
#26449=ORIENTED_EDGE ( 'NONE', *, *, #92593, .F. ) ;
#26450=VECTOR ( 'NONE', #100267, 1000.000000000000114 ) ;
#26452=CARTESIAN_POINT ( 'NONE',  ( -90.62287095715004170, -23.47596703998600631, 11.44779298504227860 ) ) ;
#26453=CARTESIAN_POINT ( 'NONE',  ( -122.6228709571500417, -29.50250243563736774, 8.947779886222134493 ) ) ;
#26454=CARTESIAN_POINT ( 'NONE',  ( -92.62287095715004170, -24.50321055353805377, 9.387540953477525818 ) ) ;
#26455=PLANE ( 'NONE',  #73985 ) ;
#26456=CARTESIAN_POINT ( 'NONE',  ( -103.5228709571500758, -24.65952944569304606, 1.056160979905702346 ) ) ;
#26458=AXIS2_PLACEMENT_3D ( 'NONE', #36379, #67845, #91158 ) ;
#26459=CARTESIAN_POINT ( 'NONE',  ( -98.87475183225456021, -25.25978491487772004, 3.590542621692357717 ) ) ;
#26460=EDGE_LOOP ( 'NONE', ( #88864, #71275, #50086, #39288 ) ) ;
#26461=CARTESIAN_POINT ( 'NONE',  ( -19.38859340154505873, -6.080128201517944753, 11.49999999999998934 ) ) ;
#26462=VECTOR ( 'NONE', #57859, 1000.000000000000114 ) ;
#26463=VERTEX_POINT ( 'NONE', #66211 ) ;
#26464=CARTESIAN_POINT ( 'NONE',  ( -12.73177969873712279, -19.06072230859735939, 11.49999999999998934 ) ) ;
#26465=CARTESIAN_POINT ( 'NONE',  ( -32.48910047119002087, -24.34968618360933590, 0.1864209137778856384 ) ) ;
#26466=CARTESIAN_POINT ( 'NONE',  ( -127.5208712269004252, -24.66019654487200441, 8.947790411086106843 ) ) ;
#26467=EDGE_LOOP ( 'NONE', ( #62289, #79204, #44599, #50825 ) ) ;
#26468=CARTESIAN_POINT ( 'NONE',  ( -59.49820692736138028, -24.35071581493543391, 9.817618358456035921 ) ) ;
#26471=CARTESIAN_POINT ( 'NONE',  ( -30.47287095715006444, -24.38745407128210019, 0.3244550880798094949 ) ) ;
#26472=CARTESIAN_POINT ( 'NONE',  ( -19.96038302963917488, -7.207760892512529161, 11.49999999999999645 ) ) ;
#26473=CARTESIAN_POINT ( 'NONE',  ( 17.03105324785762420, 14.15717209551829647, 11.49999999999998934 ) ) ;
#26475=CARTESIAN_POINT ( 'NONE',  ( 18.07347782881280907, 9.871946371954690491, 11.49999999999998934 ) ) ;
#26477=DIRECTION ( 'NONE',  ( 3.773278334444167608E-23, -1.000000000000000000, 0.000000000000000000 ) ) ;
#26478=VERTEX_POINT ( 'NONE', #58576 ) ;
#26481=ORIENTED_EDGE ( 'NONE', *, *, #14979, .F. ) ;
#26482=ORIENTED_EDGE ( 'NONE', *, *, #83320, .F. ) ;
#26485=FACE_OUTER_BOUND ( 'NONE', #7492, .T. ) ;
#26486=CARTESIAN_POINT ( 'NONE',  ( -91.62287095715004170, -24.34917612406837861, 0.1852690917426654815 ) ) ;
#26487=CARTESIAN_POINT ( 'NONE',  ( -10.32638548400381673, 17.97674989526738898, -1.500000000000002220 ) ) ;
#26488=CARTESIAN_POINT ( 'NONE',  ( 21.03555826204448209, -5.341079136732027166, 11.49999999999999645 ) ) ;
#26493=CARTESIAN_POINT ( 'NONE',  ( -14.11974515630795501, -17.41659395067913962, -1.500000000000002220 ) ) ;
#26495=CARTESIAN_POINT ( 'NONE',  ( -58.22287095715005734, -23.47596703998600276, 11.44779298504227683 ) ) ;
#26496=ORIENTED_EDGE ( 'NONE', *, *, #97973, .F. ) ;
#26500=ORIENTED_EDGE ( 'NONE', *, *, #30820, .T. ) ;
#26501=EDGE_LOOP ( 'NONE', ( #46211, #9993, #88373, #65001 ) ) ;
#26502=CARTESIAN_POINT ( 'NONE',  ( -87.62287095715004170, -24.50216790748098816, 0.6166512839513664801 ) ) ;
#26504=VERTEX_POINT ( 'NONE', #43357 ) ;
#26505=CARTESIAN_POINT ( 'NONE',  ( -17.82860346875387947, 11.52481846644873187, -1.500000000000002220 ) ) ;
#26506=ORIENTED_EDGE ( 'NONE', *, *, #8092, .T. ) ;
#26507=CARTESIAN_POINT ( 'NONE',  ( -88.60252077244210511, -23.48783264082477018, -1.443836473390093467 ) ) ;
#26508=CARTESIAN_POINT ( 'NONE',  ( 4.989390281198801347, -21.28523531580253803, -1.500000000000002220 ) ) ;
#26509=CARTESIAN_POINT ( 'NONE',  ( -52.58731372522222358, -24.35071581493542681, 9.817618358456035921 ) ) ;
#26510=CARTESIAN_POINT ( 'NONE',  ( -40.55984193903805846, -25.28892422735297174, 3.296901279442651322 ) ) ;
#26512=CARTESIAN_POINT ( 'NONE',  ( 20.64021973274467570, 7.317367941133321452, -1.500000000000002220 ) ) ;
#26514=EDGE_LOOP ( 'NONE', ( #23071, #4753, #62996, #89526 ) ) ;
#26516=CARTESIAN_POINT ( 'NONE',  ( -121.5228709571500048, -23.47593901973090524, -1.443836447538996204 ) ) ;
#26517=ORIENTED_EDGE ( 'NONE', *, *, #79662, .T. ) ;
#26519=CARTESIAN_POINT ( 'NONE',  ( -30.59820534742401676, -24.75468375855055925, 1.373310540286951209 ) ) ;
#26520=ORIENTED_EDGE ( 'NONE', *, *, #74519, .T. ) ;
#26523=CARTESIAN_POINT ( 'NONE',  ( -20.82729772986975547, -4.079710536234080642, 11.49999999999998934 ) ) ;
#26524=DIRECTION ( 'NONE',  ( -1.000000000000000000, -3.773278334444166432E-23, -8.201307841325785021E-29 ) ) ;
#26527=DIRECTION ( 'NONE',  ( -0.000000000000000000, 2.173523156925979552E-06, -0.9999999999976378895 ) ) ;
#26529=CARTESIAN_POINT ( 'NONE',  ( -19.27395093635484713, 2.380100695660296140, 11.49999999999998934 ) ) ;
#26532=CARTESIAN_POINT ( 'NONE',  ( -19.52990877098713796, 1.257015143768854815, 11.49999999999999645 ) ) ;
#26534=B_SPLINE_CURVE_WITH_KNOTS ( 'NONE', 3,
 ( #10357, #97095, #72273, #50932 ),
 .UNSPECIFIED., .F., .F.,
 ( 4, 4 ),
 ( 0.000000000000000000, 9.999999999998900014E-05 ),
 .UNSPECIFIED. ) ;
#26535=AXIS2_PLACEMENT_3D ( 'NONE', #72207, #78290, #8798 ) ;
#26536=EDGE_CURVE ( 'NONE', #71288, #909, #62377, .T. ) ;
#26537=CARTESIAN_POINT ( 'NONE',  ( -42.55620429048338593, -23.48786465467240347, 11.44779295918255180 ) ) ;
#26538=VERTEX_POINT ( 'NONE', #59581 ) ;
#26539=CARTESIAN_POINT ( 'NONE',  ( -97.62287095715005592, -24.33832256526969218, 0.1851278514119914509 ) ) ;
#26540=CARTESIAN_POINT ( 'NONE',  ( -75.62287095715005592, -25.00158670708909625, 2.256160236439166855 ) ) ;
#26542=CARTESIAN_POINT ( 'NONE',  ( -81.60636161561390622, -25.24813873414510113, 7.020724594378081385 ) ) ;
#26543=CARTESIAN_POINT ( 'NONE',  ( 19.16472379399037251, -4.548241762842377689, -1.500000000000002220 ) ) ;
#26544=ORIENTED_EDGE ( 'NONE', *, *, #40250, .F. ) ;
#26545=EDGE_CURVE ( 'NONE', #46271, #12512, #73305, .T. ) ;
#26551=CARTESIAN_POINT ( 'NONE',  ( -106.5562042904834357, -24.64965694238575722, 8.947790433994187609 ) ) ;
#26552=DIRECTION ( 'NONE',  ( -3.773278334453079618E-23, 0.9999999999976377785, 2.173523156925979975E-06 ) ) ;
#26553=CARTESIAN_POINT ( 'NONE',  ( -69.62287095715007013, -24.50216790748100593, 0.6166512839513600408 ) ) ;
#26554=CARTESIAN_POINT ( 'NONE',  ( -105.6228709571500417, -24.52323809116984066, 9.355190652339416602 ) ) ;
#26555=CARTESIAN_POINT ( 'NONE',  ( -81.90208261351192220, -25.29489613318244423, 6.057562805997258160 ) ) ;
#26557=B_SPLINE_CURVE_WITH_KNOTS ( 'NONE', 3,
 ( #57392, #17298, #47257, #95428 ),
 .UNSPECIFIED., .F., .F.,
 ( 4, 4 ),
 ( 0.000000000000000000, 9.999999999998897304E-05 ),
 .UNSPECIFIED. ) ;
#26560=CARTESIAN_POINT ( 'NONE',  ( 8.914523860536577970, -17.85282776015759154, 11.49999999999998934 ) ) ;
#26561=EDGE_CURVE ( 'NONE', #35855, #93616, #37034, .T. ) ;
#26562=AXIS2_PLACEMENT_3D ( 'NONE', #16332, #85342, #14325 ) ;
#26563=CARTESIAN_POINT ( 'NONE',  ( -75.49128105450554926, -24.92592662359561118, 8.075495903018000021 ) ) ;
#26564=CARTESIAN_POINT ( 'NONE',  ( -19.70454523906213495, -2.556213046838741842, -1.500000000000002220 ) ) ;
#26565=ORIENTED_EDGE ( 'NONE', *, *, #63019, .F. ) ;
#26566=CARTESIAN_POINT ( 'NONE',  ( -120.6228709571500417, -23.48783264082479505, -1.443836473390058384 ) ) ;
#26568=CARTESIAN_POINT ( 'NONE',  ( -125.5228709571500900, -24.14321612903116332, -0.2833117244521576872 ) ) ;
#26571=CARTESIAN_POINT ( 'NONE',  ( -15.88994834598175387, -13.44966708658631838, 11.49999999999999645 ) ) ;
#26573=CARTESIAN_POINT ( 'NONE',  ( -50.81585168191263335, -25.19418440451270058, 3.360232408535756665 ) ) ;
#26574=CARTESIAN_POINT ( 'NONE',  ( 16.54545882101025711, 15.75737887292823558, 11.49999999999999645 ) ) ;
#26575=ORIENTED_EDGE ( 'NONE', *, *, #72315, .F. ) ;
#26576=CARTESIAN_POINT ( 'NONE',  ( -103.5228709571500758, -23.48786465467241769, 11.44779295918254114 ) ) ;
#26577=PLANE ( 'NONE',  #93813 ) ;
#26579=CARTESIAN_POINT ( 'NONE',  ( 18.08294815051442583, 9.098846914115775064, -1.500000000000002220 ) ) ;
#26581=CARTESIAN_POINT ( 'NONE',  ( -80.62287095715005592, -29.50248528299804818, 1.056150453629038477 ) ) ;
#26582=DIRECTION ( 'NONE',  ( -3.773278334453079030E-23, 0.9999999999976377785, 2.173523156925979128E-06 ) ) ;
#26585=CARTESIAN_POINT ( 'NONE',  ( -79.48419046236253394, -25.30823799978809419, 5.428935451781088162 ) ) ;
#26588=CARTESIAN_POINT ( 'NONE',  ( 19.27460657395150889, -5.330843762518559181, -1.500000000000002220 ) ) ;
#26589=CARTESIAN_POINT ( 'NONE',  ( -17.93810645791062441, 10.97360191750010827, 11.49999999999999645 ) ) ;
#26591=CARTESIAN_POINT ( 'NONE',  ( -93.52287095715007581, -23.73934037231756733, 11.05740245334328975 ) ) ;
#26592=CARTESIAN_POINT ( 'NONE',  ( 21.54648482299927181, -4.703075207800759827, -1.500000000000002220 ) ) ;
#26595=CARTESIAN_POINT ( 'NONE',  ( -97.52287095715006160, -29.50248528299804818, 1.056150453629042030 ) ) ;
#26597=FACE_OUTER_BOUND ( 'NONE', #83399, .T. ) ;
#26598=DIRECTION ( 'NONE',  ( 0.000000000000000000, -0.9999999999976377785, -2.173523156925979975E-06 ) ) ;
#26599=VERTEX_POINT ( 'NONE', #35741 ) ;
#26602=B_SPLINE_CURVE_WITH_KNOTS ( 'NONE', 3,
 ( #84799, #29510, #5679, #59987 ),
 .UNSPECIFIED., .F., .F.,
 ( 4, 4 ),
 ( 0.000000000000000000, 1.000000000000000000 ),
 .UNSPECIFIED. ) ;
#26603=CARTESIAN_POINT ( 'NONE',  ( -100.6747599127204040, -25.27404634170540376, 2.849795293083101200 ) ) ;
#26605=CARTESIAN_POINT ( 'NONE',  ( -1.764913036440812322, 20.45846032914734280, -1.500000000000002220 ) ) ;
#26607=LINE ( 'NONE', #57569, #2442 ) ;
#26608=CARTESIAN_POINT ( 'NONE',  ( -97.62287095715005592, -23.48786465467241058, 11.44779295918254114 ) ) ;
#26610=CARTESIAN_POINT ( 'NONE',  ( -22.12323335113916301, -3.008119206214963981, -1.500000000000002220 ) ) ;
#26612=CARTESIAN_POINT ( 'NONE',  ( -121.6228709571500559, -23.47596703998600631, 11.44779298504227683 ) ) ;
#26615=CARTESIAN_POINT ( 'NONE',  ( -51.69888143875354558, -25.26742185460100387, 4.038564875323308989 ) ) ;
#26617=CARTESIAN_POINT ( 'NONE',  ( -19.85847575633505713, -6.422239212204448044, -1.500000000000002220 ) ) ;
#26618=ORIENTED_EDGE ( 'NONE', *, *, #31811, .T. ) ;
#26619=VECTOR ( 'NONE', #49404, 1000.000000000000114 ) ;
#26620=DIRECTION ( 'NONE',  ( -3.773278334444167608E-23, 1.000000000000000000, 0.000000000000000000 ) ) ;
#26623=ORIENTED_EDGE ( 'NONE', *, *, #10765, .T. ) ;
#26624=CARTESIAN_POINT ( 'NONE',  ( -69.03624148920614800, -25.03149190493494203, 6.724186720489000457 ) ) ;
#26625=CARTESIAN_POINT ( 'NONE',  ( -20.42954818520503935, 5.180689535515515587, -1.500000000000002220 ) ) ;
#26626=ORIENTED_EDGE ( 'NONE', *, *, #20896, .T. ) ;
#26627=CARTESIAN_POINT ( 'NONE',  ( -114.6228709571500559, -23.72773821059536559, 11.05748984161097503 ) ) ;
#26629=DIRECTION ( 'NONE',  ( 0.000000000000000000, -2.173523156925979552E-06, 0.9999999999976378895 ) ) ;
#26630=EDGE_CURVE ( 'NONE', #20641, #50993, #7910, .T. ) ;
#26631=CARTESIAN_POINT ( 'NONE',  ( -101.8751956322788317, -25.25419332119572857, 6.541289853642102692 ) ) ;
#26633=CARTESIAN_POINT ( 'NONE',  ( -20.56447267657262401, 6.860157381912782348, -1.500000000000002220 ) ) ;
#26634=CARTESIAN_POINT ( 'NONE',  ( -81.45245898465185519, -25.12224243742947749, 6.419336199521627151 ) ) ;
#26635=CARTESIAN_POINT ( 'NONE',  ( 16.16129659511371131, 15.28805624652528472, 11.49999999999999645 ) ) ;
#26636=ORIENTED_EDGE ( 'NONE', *, *, #57917, .T. ) ;
#26637=CARTESIAN_POINT ( 'NONE',  ( -51.48368152949297638, -25.24728876902798902, 5.903371821033232436 ) ) ;
#26640=VERTEX_POINT ( 'NONE', #96623 ) ;
#26648=CARTESIAN_POINT ( 'NONE',  ( -107.5228709571501042, -23.73907113217658704, -1.053371485781485317 ) ) ;
#26649=CARTESIAN_POINT ( 'NONE',  ( -32.62287095715004881, -23.48783264082477729, -1.443836473390074371 ) ) ;
#26651=CARTESIAN_POINT ( 'NONE',  ( -130.5728709571500303, -24.15356421501153861, -0.4487796565293491469 ) ) ;
#26652=CARTESIAN_POINT ( 'NONE',  ( 4.981011153104904388, 21.88276397462241363, -1.500000000000002220 ) ) ;
#26654=ORIENTED_EDGE ( 'NONE', *, *, #7158, .T. ) ;
#26655=CARTESIAN_POINT ( 'NONE',  ( -112.5569623894730569, -23.73791477778912551, 11.05961554403169878 ) ) ;
#26656=CARTESIAN_POINT ( 'NONE',  ( -94.55792968542381516, -23.73791477778911840, 11.05961554403170588 ) ) ;
#26658=DIRECTION ( 'NONE',  ( -3.773278334453079618E-23, 0.9999999999976377785, 2.173523156925979975E-06 ) ) ;
#26659=CARTESIAN_POINT ( 'NONE',  ( -63.92071404197809414, -24.75179208683297105, 8.640809912072082710 ) ) ;
#26660=CARTESIAN_POINT ( 'NONE',  ( 3.881049643139886207, -19.21785841795820104, 11.49999999999998934 ) ) ;
#26662=ORIENTED_EDGE ( 'NONE', *, *, #19687, .T. ) ;
#26663=VECTOR ( 'NONE', #11310, 1000.000000000000114 ) ;
#26664=CARTESIAN_POINT ( 'NONE',  ( -17.55493245422511350, -12.44833567967518029, 11.49999999999998934 ) ) ;
#26666=CARTESIAN_POINT ( 'NONE',  ( -114.5228709571500758, -23.72747288104470798, -1.053458166803225238 ) ) ;
#26667=CARTESIAN_POINT ( 'NONE',  ( -70.52287095715007581, -23.47596703998600631, 11.44779298504228748 ) ) ;
#26668=B_SPLINE_CURVE_WITH_KNOTS ( 'NONE', 3,
 ( #49292, #18322, #48789, #73120 ),
 .UNSPECIFIED., .F., .F.,
 ( 4, 4 ),
 ( 0.9194398632183746756, 0.9204406102591400352 ),
 .UNSPECIFIED. ) ;
#26670=CARTESIAN_POINT ( 'NONE',  ( 0.5590224530292132732, -22.91010021869659852, -1.500000000000002220 ) ) ;
#26672=EDGE_CURVE ( 'NONE', #69394, #67776, #99107, .T. ) ;
#26676=CARTESIAN_POINT ( 'NONE',  ( 1.781536345648733199, 20.00535218256611358, 11.49999999999999645 ) ) ;
#26677=CARTESIAN_POINT ( 'NONE',  ( -112.6228709571500417, -24.65952944569304961, 1.056160979905702346 ) ) ;
#26680=CARTESIAN_POINT ( 'NONE',  ( -102.5228709571500758, -24.64898659630367916, 1.056161002820829697 ) ) ;
#26681=PLANE ( 'NONE',  #26737 ) ;
#26682=CARTESIAN_POINT ( 'NONE',  ( -19.84341114293531305, -1.032944114202840824, -1.500000000000002220 ) ) ;
#26683=ADVANCED_FACE ( 'NONE', ( #83391 ), #60583, .T. ) ;
#26685=CARTESIAN_POINT ( 'NONE',  ( -5.084378373094740944, 19.06436389234985285, -1.500000000000002220 ) ) ;
#26686=CARTESIAN_POINT ( 'NONE',  ( -75.52287095715007581, -23.48786465467241769, 11.44779295918254469 ) ) ;
#26687=ADVANCED_FACE ( 'NONE', ( #45349 ), #46334, .F. ) ;
#26688=ADVANCED_FACE ( 'NONE', ( #77265 ), #19941, .T. ) ;
#26691=CARTESIAN_POINT ( 'NONE',  ( -20.25002411749221665, -3.895867502427604379, 11.49999999999999645 ) ) ;
#26694=CARTESIAN_POINT ( 'NONE',  ( -11.11902432501355342, 19.77583997595719367, 11.49999999999999645 ) ) ;
#26695=VERTEX_POINT ( 'NONE', #80663 ) ;
#26696=CARTESIAN_POINT ( 'NONE',  ( -115.5562042904833788, -25.00182538069145721, 7.747789668545097541 ) ) ;
#26697=CARTESIAN_POINT ( 'NONE',  ( -109.6228709571500559, -23.47596703998600631, 11.44779298504227860 ) ) ;
#26698=CARTESIAN_POINT ( 'NONE',  ( -127.5228709571500616, -24.50321055353805377, 9.387540953477508054 ) ) ;
#26703=CARTESIAN_POINT ( 'NONE',  ( -30.49308942697465952, -23.47593901973084485, -1.443836476861628970 ) ) ;
#26704=CARTESIAN_POINT ( 'NONE',  ( -22.55118551311790753, 3.560990644294375063, -1.500000000000002220 ) ) ;
#26705=DIRECTION ( 'NONE',  ( 0.000000000000000000, 0.9999999999976377785, 2.173523156925979128E-06 ) ) ;
#26707=CARTESIAN_POINT ( 'NONE',  ( -63.50971770550398077, -23.96169478059713143, 10.65365249895718236 ) ) ;
#26708=CARTESIAN_POINT ( 'NONE',  ( -21.16806448877717628, 7.570426553894726851, 11.49999999999999645 ) ) ;
#26710=CARTESIAN_POINT ( 'NONE',  ( -43.53440695141820527, -24.51314013834316086, 0.6176544820404143987 ) ) ;
#26711=CARTESIAN_POINT ( 'NONE',  ( -1.948345350117603125, -21.87844622001750139, -1.500000000000002220 ) ) ;
#26712=CARTESIAN_POINT ( 'NONE',  ( -111.6235230694679785, -24.65952944569305316, 1.056160979905705455 ) ) ;
#26713=CARTESIAN_POINT ( 'NONE',  ( -29.21998272650427708, -24.79699891632823494, 5.646414127112506343 ) ) ;
#26714=ORIENTED_EDGE ( 'NONE', *, *, #12893, .T. ) ;
#26716=CARTESIAN_POINT ( 'NONE',  ( -107.5228709571501184, -24.33927499327856125, 9.819080762295811837 ) ) ;
#26718=ORIENTED_EDGE ( 'NONE', *, *, #12649, .T. ) ;
#26719=CARTESIAN_POINT ( 'NONE',  ( -45.52287095715004028, -24.62226745350437795, 0.9660975649728088532 ) ) ;
#26720=CARTESIAN_POINT ( 'NONE',  ( 1.819314030819549233, -20.42850443921780013, -1.500000000000002220 ) ) ;
#26722=B_SPLINE_CURVE_WITH_KNOTS ( 'NONE', 3,
 ( #50985, #11908, #42386, #42875, #73805, #19015, #74308, #4800 ),
 .UNSPECIFIED., .F., .F.,
 ( 4, 2, 2, 4 ),
 ( -0.001224873891641433451, -0.0002244903592271139166, 0.0007758931731872056176, 0.002776660238015840349 ),
 .UNSPECIFIED. ) ;
#26723=ORIENTED_EDGE ( 'NONE', *, *, #95826, .F. ) ;
#26724=ORIENTED_EDGE ( 'NONE', *, *, #64133, .F. ) ;
#26725=CARTESIAN_POINT ( 'NONE',  ( -80.54756436351547677, -25.13342022318803615, 7.100032767599389061 ) ) ;
#26726=CARTESIAN_POINT ( 'NONE',  ( 19.36532470938277228, 12.59445105952145738, -1.500000000000002220 ) ) ;
#26727=CARTESIAN_POINT ( 'NONE',  ( -104.5928576678435746, -23.96169478059713853, 10.65365249895717525 ) ) ;
#26728=CARTESIAN_POINT ( 'NONE',  ( 18.91379238805564356, 7.493326543281090935, -1.500000000000002220 ) ) ;
#26731=CARTESIAN_POINT ( 'NONE',  ( -50.78270459440467732, -25.12977507029983926, 2.884057882057353694 ) ) ;
#26732=CARTESIAN_POINT ( 'NONE',  ( -105.5874393031439809, -24.73486907724918282, 1.287355809206962576 ) ) ;
#26734=ORIENTED_EDGE ( 'NONE', *, *, #3097, .T. ) ;
#26735=CARTESIAN_POINT ( 'NONE',  ( -29.10059600771309007, -24.76881121394164964, 3.504325771330080386 ) ) ;
#26737=AXIS2_PLACEMENT_3D ( 'NONE', #81471, #11945, #35299 ) ;
#26739=CARTESIAN_POINT ( 'NONE',  ( -20.13249939377427111, -5.111880259578561514, 11.49999999999998934 ) ) ;
#26740=ORIENTED_EDGE ( 'NONE', *, *, #91809, .T. ) ;
#26742=ORIENTED_EDGE ( 'NONE', *, *, #7350, .F. ) ;
#26744=CARTESIAN_POINT ( 'NONE',  ( -77.52287095715006160, -24.33832256527049154, 0.1851278514138615938 ) ) ;
#26745=CARTESIAN_POINT ( 'NONE',  ( -102.6228709571500985, -24.33832256526968862, 0.1851278514119935603 ) ) ;
#26746=ORIENTED_EDGE ( 'NONE', *, *, #70402, .F. ) ;
#26747=VERTEX_POINT ( 'NONE', #18264 ) ;
#26750=CARTESIAN_POINT ( 'NONE',  ( -43.49938052968830959, -24.15620529776627734, 10.23563542870661003 ) ) ;
#26751=CARTESIAN_POINT ( 'NONE',  ( -19.65368394218270254, -10.04821906498216499, 11.49999999999999645 ) ) ;
#26753=CARTESIAN_POINT ( 'NONE',  ( -47.62287095715005592, -24.35013146730204170, 9.818937971375113705 ) ) ;
#26754=CARTESIAN_POINT ( 'NONE',  ( 21.16457415087624128, -7.944649954575952577, 11.49999999999998934 ) ) ;
#26759=ORIENTED_EDGE ( 'NONE', *, *, #10032, .T. ) ;
#26761=EDGE_CURVE ( 'NONE', #34988, #66705, #95885, .T. ) ;
#26763=VECTOR ( 'NONE', #27947, 1000.000000000000114 ) ;
#26764=CARTESIAN_POINT ( 'NONE',  ( -36.55620429048339304, -24.64965694238575011, 8.947790433994200043 ) ) ;
#26766=CARTESIAN_POINT ( 'NONE',  ( 9.297385241821217505, 19.04214385377821017, 11.49999999999998934 ) ) ;
#26768=FACE_OUTER_BOUND ( 'NONE', #73322, .T. ) ;
#26769=CARTESIAN_POINT ( 'NONE',  ( -22.27612280437926273, 0.2766752662994830247, -1.500000000000002220 ) ) ;
#26770=DIRECTION ( 'NONE',  ( 0.000000000000000000, -0.9999999999976377785, -2.173523156925979975E-06 ) ) ;
#26771=ADVANCED_FACE ( 'NONE', ( #41616 ), #71751, .T. ) ;
#26773=VERTEX_POINT ( 'NONE', #88788 ) ;
#26774=CARTESIAN_POINT ( 'NONE',  ( -110.5895376238167387, -23.47596703998600631, 11.44779298504227683 ) ) ;
#26776=VECTOR ( 'NONE', #76240, 1000.000000000000114 ) ;
#26777=CARTESIAN_POINT ( 'NONE',  ( -36.58084380204805086, -24.51419770103156637, 9.386484678747175181 ) ) ;
#26779=EDGE_CURVE ( 'NONE', #99833, #80512, #32168, .T. ) ;
#26780=CARTESIAN_POINT ( 'NONE',  ( 13.27039818535887505, -14.28956163997708906, -1.500000000000002220 ) ) ;
#26781=CARTESIAN_POINT ( 'NONE',  ( 19.99082695160776169, -7.785253749782737209, -1.500000000000002220 ) ) ;
#26782=CARTESIAN_POINT ( 'NONE',  ( -26.25707451207771470, -24.57999642328221768, 2.297367441281741751 ) ) ;
#26783=LINE ( 'NONE', #41513, #92421 ) ;
#26784=DIRECTION ( 'NONE',  ( 3.773278334444166432E-23, -1.000000000000000000, 0.000000000000000000 ) ) ;
#26785=CARTESIAN_POINT ( 'NONE',  ( -19.53289989604362376, -11.71160353944097920, -1.500000000000002220 ) ) ;
#26790=CARTESIAN_POINT ( 'NONE',  ( -10.02925392579303576, -17.20239368982820238, 11.49999999999999645 ) ) ;
#26792=DIRECTION ( 'NONE',  ( -3.773278334453080206E-23, 0.9999999999976377785, 2.173523156925979975E-06 ) ) ;
#26793=CARTESIAN_POINT ( 'NONE',  ( -76.55620429048340725, -23.47596703998600276, 11.44779298504227683 ) ) ;
#26794=VERTEX_POINT ( 'NONE', #98369 ) ;
#26795=CARTESIAN_POINT ( 'NONE',  ( -103.6228709571500701, -23.48783264082478794, -1.443836473390062158 ) ) ;
#26798=CARTESIAN_POINT ( 'NONE',  ( 12.10466045530642631, 18.00204671274030233, 11.49999999999998934 ) ) ;
#26799=CARTESIAN_POINT ( 'NONE',  ( -56.59303884526941175, -24.15620529776628445, 10.23563542870660648 ) ) ;
#26800=CARTESIAN_POINT ( 'NONE',  ( -16.58133674543539371, -10.29093563426468450, -1.500000000000002220 ) ) ;
#26802=ADVANCED_FACE ( 'NONE', ( #59835 ), #20249, .T. ) ;
#26803=ORIENTED_EDGE ( 'NONE', *, *, #81296, .T. ) ;
#26805=B_SPLINE_CURVE_WITH_KNOTS ( 'NONE', 3,
 ( #81692, #12164, #82180, #13159 ),
 .UNSPECIFIED., .F., .F.,
 ( 4, 4 ),
 ( 0.000000000000000000, 0.0001000000000000028644 ),
 .UNSPECIFIED. ) ;
#26807=DIRECTION ( 'NONE',  ( 0.2009441437208800141, 0.000000000000000000, -0.9796027006415827243 ) ) ;
#26808=CARTESIAN_POINT ( 'NONE',  ( 19.60162835767302880, 5.811842276320244416, 11.49999999999999645 ) ) ;
#26809=CARTESIAN_POINT ( 'NONE',  ( -40.62287095715005592, -29.50250786944525672, 11.44777988621624232 ) ) ;
#26813=CARTESIAN_POINT ( 'NONE',  ( -39.46304919600096639, -25.28892577674529463, 4.009749604779731413 ) ) ;
#26815=CARTESIAN_POINT ( 'NONE',  ( -109.5521161159935275, -24.34968618360934300, 0.1864209137778879422 ) ) ;
#26817=CARTESIAN_POINT ( 'NONE',  ( -79.73149462243459595, -25.14083923594767356, 2.947789366383930965 ) ) ;
#26818=CARTESIAN_POINT ( 'NONE',  ( -5.713817535623205046, 22.21719745612757535, 11.49999999999999645 ) ) ;
#26819=CARTESIAN_POINT ( 'NONE',  ( 21.04450177026006230, 8.645109164175620364, 11.49999999999998934 ) ) ;
#26820=CARTESIAN_POINT ( 'NONE',  ( -71.04002682610065733, -25.08030589124952314, 7.384199749201091123 ) ) ;
#26821=CARTESIAN_POINT ( 'NONE',  ( -40.52287095715005449, -24.62226745350442059, 0.9660975649729506287 ) ) ;
#26822=CARTESIAN_POINT ( 'NONE',  ( -90.60545780893913559, -23.48783264082477018, -1.443836473390091912 ) ) ;
#26824=DIRECTION ( 'NONE',  ( -3.773278334444166432E-23, 1.000000000000000000, 0.000000000000000000 ) ) ;
#26825=AXIS2_PLACEMENT_3D ( 'NONE', #95183, #95684, #57635 ) ;
#26826=CARTESIAN_POINT ( 'NONE',  ( -9.708950231915746798, -19.59419465507263070, -1.500000000000002220 ) ) ;
#26827=CARTESIAN_POINT ( 'NONE',  ( -74.52287095715011844, -24.33832256527049509, 0.1851278514138617326 ) ) ;
#26829=B_SPLINE_CURVE_WITH_KNOTS ( 'NONE', 3,
 ( #81286, #20366, #98991, #97506 ),
 .UNSPECIFIED., .F., .F.,
 ( 4, 4 ),
 ( 0.000000000000000000, 9.999999999998897304E-05 ),
 .UNSPECIFIED. ) ;
#26830=CARTESIAN_POINT ( 'NONE',  ( -103.5895376238167103, -24.66019654487199730, 8.947790411086115725 ) ) ;
#26831=CARTESIAN_POINT ( 'NONE',  ( -120.6228709571500275, -23.84047902841603062, -0.8780736468305480047 ) ) ;
#26833=ORIENTED_EDGE ( 'NONE', *, *, #99800, .F. ) ;
#26834=CARTESIAN_POINT ( 'NONE',  ( -10.82153711268468932, 17.32902648900640230, -1.500000000000002220 ) ) ;
#26837=ORIENTED_EDGE ( 'NONE', *, *, #30640, .T. ) ;
#26840=CARTESIAN_POINT ( 'NONE',  ( -19.18584950847915493, -12.73052202388904952, 11.49999999999998934 ) ) ;
#26842=CARTESIAN_POINT ( 'NONE',  ( -11.96439459519798554, -16.23097265130270728, -1.500000000000002220 ) ) ;
#26843=ORIENTED_EDGE ( 'NONE', *, *, #87587, .T. ) ;
#26846=AXIS2_PLACEMENT_3D ( 'NONE', #84746, #17, #8632 ) ;
#26847=CARTESIAN_POINT ( 'NONE',  ( -85.62287095715005592, -29.50250786944525672, 11.44777988621623344 ) ) ;
#26848=FACE_OUTER_BOUND ( 'NONE', #36321, .T. ) ;
#26849=CARTESIAN_POINT ( 'NONE',  ( -21.18999663186871274, 2.814949255606389311, 11.49999999999999645 ) ) ;
#26850=ORIENTED_EDGE ( 'NONE', *, *, #17701, .T. ) ;
#26851=CARTESIAN_POINT ( 'NONE',  ( -111.9545715455114987, -29.50249917535260380, 7.447779886225679213 ) ) ;
#26853=CARTESIAN_POINT ( 'NONE',  ( 10.43072250204971851, -19.66636941823637841, 11.49999999999998934 ) ) ;
#26854=CARTESIAN_POINT ( 'NONE',  ( 0.1934390699377774303, 20.68474938276070318, -1.500000000000002220 ) ) ;
#26855=ORIENTED_EDGE ( 'NONE', *, *, #4094, .F. ) ;
#26857=ORIENTED_EDGE ( 'NONE', *, *, #70660, .F. ) ;
#26859=CARTESIAN_POINT ( 'NONE',  ( -56.52287095715005449, -23.47593901973090169, -1.443836447538996870 ) ) ;
#26860=VERTEX_POINT ( 'NONE', #83650 ) ;
#26863=CARTESIAN_POINT ( 'NONE',  ( -4.092705237139750984, -20.55955383578756113, -1.500000000000002220 ) ) ;
#26864=CARTESIAN_POINT ( 'NONE',  ( -21.08706934527708654, 5.832127334627817739, 11.49999999999999645 ) ) ;
#26865=EDGE_CURVE ( 'NONE', #22696, #73872, #59864, .T. ) ;
#26866=CARTESIAN_POINT ( 'NONE',  ( -73.49608911756305929, -24.66019654487200441, 8.947790411086119278 ) ) ;
#26867=CARTESIAN_POINT ( 'NONE',  ( -22.13300264024875119, -4.194623038110560032, 11.49999999999998934 ) ) ;
#26869=CARTESIAN_POINT ( 'NONE',  ( 2.438461900574103502, 20.79476225230834174, 11.49999999999998934 ) ) ;
#26870=CARTESIAN_POINT ( 'NONE',  ( -38.49809217028499830, -24.15543982623907127, -0.2315651400026569606 ) ) ;
#26871=DIRECTION ( 'NONE',  ( -3.773278334453079030E-23, 0.9999999999976377785, 2.173523156925979128E-06 ) ) ;
#26873=CARTESIAN_POINT ( 'NONE',  ( -91.58953762381672448, -24.64965694238407323, 8.947790433994651238 ) ) ;
#26874=ORIENTED_EDGE ( 'NONE', *, *, #54881, .T. ) ;
#26876=ORIENTED_EDGE ( 'NONE', *, *, #34681, .F. ) ;
#26877=VERTEX_POINT ( 'NONE', #28873 ) ;
#26878=CARTESIAN_POINT ( 'NONE',  ( -52.49090493470863095, -24.51314013834315375, 0.6176544820404114011 ) ) ;
#26879=ORIENTED_EDGE ( 'NONE', *, *, #67009, .T. ) ;
#26880=CARTESIAN_POINT ( 'NONE',  ( -21.25412285906045895, 3.082840150875858054, -1.500000000000002220 ) ) ;
#26881=VERTEX_POINT ( 'NONE', #21245 ) ;
#26883=CARTESIAN_POINT ( 'NONE',  ( 21.06685942672242362, 1.161445541649065882, -1.500000000000002220 ) ) ;
#26884=CARTESIAN_POINT ( 'NONE',  ( -39.52287095715006870, -24.64965694238406613, 8.947790433994205372 ) ) ;
#26886=CARTESIAN_POINT ( 'NONE',  ( -87.62287095715005592, -24.51283580621365132, 0.6167428607019791453 ) ) ;
#26887=LINE ( 'NONE', #50234, #39344 ) ;
#26888=CARTESIAN_POINT ( 'NONE',  ( -51.58953762381672448, -23.48786465467241413, 11.44779295918254824 ) ) ;
#26889=CARTESIAN_POINT ( 'NONE',  ( 7.103389721457689099, 20.86620700561973862, -1.500000000000002220 ) ) ;
#26891=CARTESIAN_POINT ( 'NONE',  ( -65.51285700265663081, -23.85049219812685806, 10.88485053497527311 ) ) ;
#26892=CARTESIAN_POINT ( 'NONE',  ( -111.6228709571500559, -23.73934037231757799, 11.05740245334328087 ) ) ;
#26894=CARTESIAN_POINT ( 'NONE',  ( -62.56627033263149684, -23.48786465467241058, 11.44779295918255002 ) ) ;
#26896=CARTESIAN_POINT ( 'NONE',  ( -80.88924702628075636, -25.29868576439400840, 4.592921234843194256 ) ) ;
#26898=CARTESIAN_POINT ( 'NONE',  ( 17.14628872753620215, 12.71262973326862245, -1.500000000000002220 ) ) ;
#26899=DIRECTION ( 'NONE',  ( 0.000000000000000000, -2.173523156925980399E-06, 0.9999999999976378895 ) ) ;
#26900=CARTESIAN_POINT ( 'NONE',  ( -113.5228709571500616, -24.64965694238408034, 8.947790433994192938 ) ) ;
#26901=CARTESIAN_POINT ( 'NONE',  ( -70.55620429048339304, -24.99156044556202616, 7.747789690856175859 ) ) ;
#26902=CARTESIAN_POINT ( 'NONE',  ( -81.31047933837676567, -25.18365442479677796, 6.723090361430874573 ) ) ;
#26903=CARTESIAN_POINT ( 'NONE',  ( 22.41689761077644860, -2.907977976681301424, -1.500000000000002220 ) ) ;
#26905=CARTESIAN_POINT ( 'NONE',  ( -33.22287095715006444, -23.47596703998600276, 11.44779298504227683 ) ) ;
#26910=CARTESIAN_POINT ( 'NONE',  ( 2.412641546452875208, 19.58572291230954221, 11.49999999999999645 ) ) ;
#26915=AXIS2_PLACEMENT_3D ( 'NONE', #66990, #91793, #7065 ) ;
#26917=CARTESIAN_POINT ( 'NONE',  ( -110.6228709571500559, -23.47593901973091235, -1.443836447538999312 ) ) ;
#26918=CARTESIAN_POINT ( 'NONE',  ( -101.1189062734182755, -25.12268525518375739, 6.916461178196335879 ) ) ;
#26919=CARTESIAN_POINT ( 'NONE',  ( -21.01067979154616694, 5.129389437380057259, 11.49999999999998934 ) ) ;
#26921=AXIS2_PLACEMENT_3D ( 'NONE', #83970, #67773, #75851 ) ;
#26922=CARTESIAN_POINT ( 'NONE',  ( -16.26263985875334228, -10.51264992557365829, -1.500000000000002220 ) ) ;
#26925=CARTESIAN_POINT ( 'NONE',  ( -81.81116923543841324, -25.20690049807753041, 6.627235307510320972 ) ) ;
#26926=ADVANCED_FACE ( 'NONE', ( #45112 ), #88814, .T. ) ;
#26927=CARTESIAN_POINT ( 'NONE',  ( 9.697495225759652726, 17.24774500829319734, -1.500000000000002220 ) ) ;
#26928=ORIENTED_EDGE ( 'NONE', *, *, #5510, .T. ) ;
#26929=CARTESIAN_POINT ( 'NONE',  ( -0.6865706486018943178, -20.24796467851281179, 11.49999999999999645 ) ) ;
#26931=ADVANCED_FACE ( 'NONE', ( #78022 ), #61336, .F. ) ;
#26933=CARTESIAN_POINT ( 'NONE',  ( -37.52287095715007581, -23.96177878511307924, 10.65340807706330573 ) ) ;
#26935=CARTESIAN_POINT ( 'NONE',  ( -31.62287095715005236, -23.48786465467240347, 11.44779295918255180 ) ) ;
#26938=CARTESIAN_POINT ( 'NONE',  ( 19.70663390988245922, 3.666079223618853966, -1.500000000000002220 ) ) ;
#26939=CARTESIAN_POINT ( 'NONE',  ( -51.58953762381672448, -23.47596703998600276, 11.44779298504227505 ) ) ;
#26940=ORIENTED_EDGE ( 'NONE', *, *, #30972, .T. ) ;
#26942=CARTESIAN_POINT ( 'NONE',  ( -50.34997525821440689, -25.31297217320124204, 4.735128272951183881 ) ) ;
#26943=CARTESIAN_POINT ( 'NONE',  ( -35.53216495579373202, -24.63355581998385091, 0.9682620441944008727 ) ) ;
#26944=CARTESIAN_POINT ( 'NONE',  ( -79.76418533285618651, -25.30522694008003270, 5.133764971034367797 ) ) ;
#26946=CARTESIAN_POINT ( 'NONE',  ( -73.64404266222578599, -23.73766607897670511, -1.055555164236457344 ) ) ;
#26950=CARTESIAN_POINT ( 'NONE',  ( 15.76184642470745700, 12.85868457875834103, -1.500000000000002220 ) ) ;
#26951=ORIENTED_EDGE ( 'NONE', *, *, #61948, .T. ) ;
#26952=CARTESIAN_POINT ( 'NONE',  ( -22.92702450682246251, 0.3551139841105944162, -1.500000000000002220 ) ) ;
#26957=CARTESIAN_POINT ( 'NONE',  ( -49.74873825466967503, -25.12215384875874591, 6.941713980050353783 ) ) ;
#26959=CARTESIAN_POINT ( 'NONE',  ( 0.06830352742921809439, -21.21198074455918814, 11.49999999999999645 ) ) ;
#26960=CARTESIAN_POINT ( 'NONE',  ( -21.14055147415990277, -6.693858341896442354, 11.49999999999998934 ) ) ;
#26961=CARTESIAN_POINT ( 'NONE',  ( -7.762539992054180438, 19.06225842855939234, -1.500000000000002220 ) ) ;
#26963=VERTEX_POINT ( 'NONE', #23747 ) ;
#26964=CARTESIAN_POINT ( 'NONE',  ( -104.5228709571500758, -29.50250243563736774, 8.947779886222138046 ) ) ;
#26966=CARTESIAN_POINT ( 'NONE',  ( -54.56747232805444270, -23.48783264082476663, -1.443836473390098130 ) ) ;
#26967=CARTESIAN_POINT ( 'NONE',  ( -126.6228709571500559, -23.73934037231758509, 11.05740245334328264 ) ) ;
#26971=ORIENTED_EDGE ( 'NONE', *, *, #51179, .T. ) ;
#26973=ORIENTED_EDGE ( 'NONE', *, *, #70660, .T. ) ;
#26975=FACE_OUTER_BOUND ( 'NONE', #25644, .T. ) ;
#26977=CARTESIAN_POINT ( 'NONE',  ( -20.31193019649481357, 4.361987795224258946, -1.500000000000002220 ) ) ;
#26978=CARTESIAN_POINT ( 'NONE',  ( -20.31635052000798325, -7.690577546848336610, 11.49999999999999645 ) ) ;
#26982=CARTESIAN_POINT ( 'NONE',  ( -115.5889431145695028, -24.63355581998384736, 0.9682620441943983192 ) ) ;
#26983=CARTESIAN_POINT ( 'NONE',  ( 20.99545381566289137, 7.807860396396394620, 11.49999999999998934 ) ) ;
#26985=B_SPLINE_CURVE_WITH_KNOTS ( 'NONE', 3,
 ( #77236, #93469, #7743, #38689, #76245, #69655 ),
 .UNSPECIFIED., .F., .F.,
 ( 4, 2, 4 ),
 ( 1.570755371634150632E-05, 0.001396183895866089488, 0.002776660238015837747 ),
 .UNSPECIFIED. ) ;
#26986=EDGE_CURVE ( 'NONE', #77983, #56862, #90041, .T. ) ;
#26987=B_SPLINE_CURVE_WITH_KNOTS ( 'NONE', 3,
 ( #11952, #89584, #42923, #80971, #34802, #20064 ),
 .UNSPECIFIED., .F., .F.,
 ( 4, 2, 4 ),
 ( 0.000000000000000000, 0.001380901958385389412, 0.002761803916770778824 ),
 .UNSPECIFIED. ) ;
#26988=CARTESIAN_POINT ( 'NONE',  ( -99.52287095715006160, -29.50250243563736774, 8.947779886222138046 ) ) ;
#26989=CARTESIAN_POINT ( 'NONE',  ( -61.58953762381672448, -24.64965694238574656, 8.947790433994201820 ) ) ;
#26991=CARTESIAN_POINT ( 'NONE',  ( -31.62287095715005236, -23.48786465467240347, 11.44779295918255180 ) ) ;
#26993=EDGE_CURVE ( 'NONE', #55188, #86370, #85179, .T. ) ;
#26996=EDGE_LOOP ( 'NONE', ( #65253, #94118, #29447, #39360 ) ) ;
#26997=FACE_OUTER_BOUND ( 'NONE', #26116, .T. ) ;
#26998=VERTEX_POINT ( 'NONE', #7529 ) ;
#26999=CARTESIAN_POINT ( 'NONE',  ( -21.08860491664495029, 2.407354197416772035, -1.500000000000002220 ) ) ;
#27001=CARTESIAN_POINT ( 'NONE',  ( -68.62287095715005592, -24.65952944569304606, 1.056160979905698794 ) ) ;
#27002=CARTESIAN_POINT ( 'NONE',  ( 4.919149715316761373, 21.27959583485438344, -1.500000000000002220 ) ) ;
#27003=CARTESIAN_POINT ( 'NONE',  ( -103.5477529696951819, -24.66019654487200086, 8.947790411086115725 ) ) ;
#27004=CARTESIAN_POINT ( 'NONE',  ( -21.72567761722203628, 6.514095075961352954, -1.500000000000002220 ) ) ;
#27005=CARTESIAN_POINT ( 'NONE',  ( -125.5228709571500616, -25.00182538069146077, 7.747789668545104647 ) ) ;
#27007=CARTESIAN_POINT ( 'NONE',  ( -20.59625928752216240, -7.366027188055905839, -1.500000000000002220 ) ) ;
#27008=CARTESIAN_POINT ( 'NONE',  ( -55.52287095715006870, -25.00182538069145011, 7.747789668545106423 ) ) ;
#27009=VERTEX_POINT ( 'NONE', #23240 ) ;
#27010=EDGE_CURVE ( 'NONE', #51976, #44200, #97411, .T. ) ;
#27011=CARTESIAN_POINT ( 'NONE',  ( -65.62287095715002749, -23.85196035786901092, -0.8779234886474904798 ) ) ;
#27012=DIRECTION ( 'NONE',  ( -1.000000000000000000, -3.773278334444167608E-23, -8.201307833595939069E-29 ) ) ;
#27013=AXIS2_PLACEMENT_3D ( 'NONE', #40463, #71412, #25222 ) ;
#27015=CARTESIAN_POINT ( 'NONE',  ( -30.60882031961203253, -24.47943607710057634, 0.5667427426393205625 ) ) ;
#27019=CARTESIAN_POINT ( 'NONE',  ( -0.06470660251384131867, -22.21232218138523606, 0.8294870405985470541 ) ) ;
#27020=CARTESIAN_POINT ( 'NONE',  ( -0.06837171988653999166, -21.26218376953697486, 11.49999999999998934 ) ) ;
#27022=CARTESIAN_POINT ( 'NONE',  ( -26.09929425038925999, -24.75186500840231218, 4.716438697959393522 ) ) ;
#27023=DIRECTION ( 'NONE',  ( 0.000000000000000000, 2.173523156925980399E-06, -0.9999999999976378895 ) ) ;
#27024=CARTESIAN_POINT ( 'NONE',  ( -31.24388727629348494, -29.50248678627064081, 1.747779886239157809 ) ) ;
#27025=CARTESIAN_POINT ( 'NONE',  ( -117.6281512103715272, -23.73791477778912551, 11.05961554403169878 ) ) ;
#27026=ORIENTED_EDGE ( 'NONE', *, *, #30299, .T. ) ;
#27027=CARTESIAN_POINT ( 'NONE',  ( 19.26631176993168282, 3.279242639417544236, 11.49999999999999645 ) ) ;
#27029=CARTESIAN_POINT ( 'NONE',  ( -55.62287095715004881, -23.48783264082478084, -1.443836473390068820 ) ) ;
#27031=ORIENTED_EDGE ( 'NONE', *, *, #62408, .T. ) ;
#27033=CARTESIAN_POINT ( 'NONE',  ( -100.4498239493576648, -25.03284467579916495, 7.563174216508126158 ) ) ;
#27036=ADVANCED_FACE ( 'NONE', ( #54224 ), #47608, .F. ) ;
#27037=CARTESIAN_POINT ( 'NONE',  ( -32.07722060962682775, -29.50250091417111520, 8.247779886223803203 ) ) ;
#27038=CARTESIAN_POINT ( 'NONE',  ( -5.193715590271882121, 18.98282465337476665, 11.49999999999998934 ) ) ;
#27040=DIRECTION ( 'NONE',  ( -3.773278334453079618E-23, 0.9999999999976377785, 2.173523156925979975E-06 ) ) ;
#27041=CARTESIAN_POINT ( 'NONE',  ( -42.62287095715004881, -24.66019654487199020, 8.947790411086135265 ) ) ;
#27042=B_SPLINE_CURVE_WITH_KNOTS ( 'NONE', 3,
 ( #97627, #59088, #82403, #43855, #41870, #19007, #20995, #29610, #5780, #37726, #15377, #68686, #84400, #91506, #14880, #36243 ),
 .UNSPECIFIED., .F., .F.,
 ( 4, 2, 2, 2, 2, 2, 2, 4 ),
 ( 0.000000000000000000, 0.0003118279254866530067, 0.0006236558509733060134, 0.0009354837764599591285, 0.001247311701946612027, 0.001870967552919916305, 0.002182795478406559988, 0.002494623403893203670 ),
 .UNSPECIFIED. ) ;
#27045=ADVANCED_FACE ( 'NONE', ( #77530 ), #61835, .T. ) ;
#27046=ORIENTED_EDGE ( 'NONE', *, *, #41009, .T. ) ;
#27049=DIRECTION ( 'NONE',  ( 1.000000000000000000, 3.773278334444166432E-23, 8.201307841325785021E-29 ) ) ;
#27050=CARTESIAN_POINT ( 'NONE',  ( -105.6228709571500559, -23.48786465467241769, 11.44779295918253759 ) ) ;
#27051=DIRECTION ( 'NONE',  ( 0.000000000000000000, 0.9999999999976377785, 2.173523156925979975E-06 ) ) ;
#27052=VECTOR ( 'NONE', #15499, 1000.000000000000114 ) ;
#27054=DIRECTION ( 'NONE',  ( -1.000000000000000000, -3.773278334444167608E-23, -8.201307833595939069E-29 ) ) ;
#27055=CARTESIAN_POINT ( 'NONE',  ( -50.62287095715006302, -24.91544648472619272, 1.928969306349232804 ) ) ;
#27056=CARTESIAN_POINT ( 'NONE',  ( 13.89251353435424363, -14.32104260081073832, -1.500000000000002220 ) ) ;
#27057=EDGE_CURVE ( 'NONE', #65344, #29538, #15091, .T. ) ;
#27058=CARTESIAN_POINT ( 'NONE',  ( -0.01312681704450994330, -22.88006303776501582, 7.008493951326582483 ) ) ;
#27059=CARTESIAN_POINT ( 'NONE',  ( -4.768723929037996356, 19.30091236029735668, -1.500000000000002220 ) ) ;
#27060=VERTEX_POINT ( 'NONE', #38978 ) ;
#27063=CARTESIAN_POINT ( 'NONE',  ( -72.52287095715007581, -24.64898659630367916, 1.056161002820824368 ) ) ;
#27065=CARTESIAN_POINT ( 'NONE',  ( -20.46667790307254009, -3.548193229090686796, 11.49999999999999645 ) ) ;
#27067=B_SPLINE_CURVE_WITH_KNOTS ( 'NONE', 3,
 ( #74877, #97233, #82497, #82007 ),
 .UNSPECIFIED., .F., .F.,
 ( 4, 4 ),
 ( 0.1906361285931100769, 0.1996425598652254996 ),
 .UNSPECIFIED. ) ;
#27069=CARTESIAN_POINT ( 'NONE',  ( -92.52287095715006160, -23.47596703998600631, 11.44779298504228393 ) ) ;
#27070=CARTESIAN_POINT ( 'NONE',  ( -22.57016884136470125, -3.422276288085174478, 11.49999999999999645 ) ) ;
#27072=CARTESIAN_POINT ( 'NONE',  ( -64.62287095715011276, -24.34917612406838572, 0.1852690917426601802 ) ) ;
#27073=FACE_OUTER_BOUND ( 'NONE', #23977, .T. ) ;
#27075=CARTESIAN_POINT ( 'NONE',  ( 9.769481717609929561, -17.74358427669893956, 11.49999999999998934 ) ) ;
#27080=ORIENTED_EDGE ( 'NONE', *, *, #58250, .T. ) ;
#27081=CARTESIAN_POINT ( 'NONE',  ( -79.44990853704386780, -25.30595284857920291, 5.490744999806991267 ) ) ;
#27082=CARTESIAN_POINT ( 'NONE',  ( -46.52287095715006160, -23.72773821059536914, 11.05748984161097326 ) ) ;
#27083=CARTESIAN_POINT ( 'NONE',  ( 20.02521558760690112, -0.9251608499524575091, -1.500000000000002220 ) ) ;
#27084=CARTESIAN_POINT ( 'NONE',  ( 18.99863377428308198, 9.053671573812124507, 11.49999999999999645 ) ) ;
#27086=CARTESIAN_POINT ( 'NONE',  ( -54.62287095715004881, -23.73934037231756022, 11.05740245334329508 ) ) ;
#27088=CARTESIAN_POINT ( 'NONE',  ( 21.39010012190943755, 5.354582491813655309, -1.500000000000002220 ) ) ;
#27089=CARTESIAN_POINT ( 'NONE',  ( -39.78092788824959314, -25.31589286589048982, 4.883081598822826663 ) ) ;
#27090=CARTESIAN_POINT ( 'NONE',  ( -60.52287095715006160, -24.99132157543083821, 2.256160258750667502 ) ) ;
#27092=CARTESIAN_POINT ( 'NONE',  ( -90.25937923781920347, -25.27880950044345454, 5.947789066509451494 ) ) ;
#27093=CARTESIAN_POINT ( 'NONE',  ( -31.62287095715005236, -23.73907113216990439, -1.053371485793236362 ) ) ;
#27097=DIRECTION ( 'NONE',  ( 3.773278334444167608E-23, -1.000000000000000000, 0.000000000000000000 ) ) ;
#27098=CARTESIAN_POINT ( 'NONE',  ( -89.55620429048339304, -23.48786465467241058, 11.44779295918253936 ) ) ;
#27100=CARTESIAN_POINT ( 'NONE',  ( -1.452656003914881477, -20.50939586048694352, -1.500000000000002220 ) ) ;
#27104=CARTESIAN_POINT ( 'NONE',  ( -80.43221577628075636, -25.31553502933635968, 4.967019755914117596 ) ) ;
#27105=CARTESIAN_POINT ( 'NONE',  ( -21.16112330106665240, 7.131417522999676351, 11.49999999999998934 ) ) ;
#27106=VECTOR ( 'NONE', #56366, 1000.000000000000114 ) ;
#27108=CARTESIAN_POINT ( 'NONE',  ( -124.6228709571500559, -23.48783264082479505, -1.443836473390058828 ) ) ;
#27109=ORIENTED_EDGE ( 'NONE', *, *, #24340, .T. ) ;
#27110=CARTESIAN_POINT ( 'NONE',  ( -32.50560601784287229, -24.86181184613565165, 1.747789954104514987 ) ) ;
#27111=CARTESIAN_POINT ( 'NONE',  ( -91.62287095715005592, -23.48786465467241769, 11.44779295918254114 ) ) ;
#27113=CARTESIAN_POINT ( 'NONE',  ( 20.25184064777635484, 4.944226511633750043, -1.500000000000002220 ) ) ;
#27115=ORIENTED_EDGE ( 'NONE', *, *, #7663, .T. ) ;
#27117=ORIENTED_EDGE ( 'NONE', *, *, #49399, .T. ) ;
#27120=ORIENTED_EDGE ( 'NONE', *, *, #95271, .F. ) ;
#27121=CARTESIAN_POINT ( 'NONE',  ( -120.6228709571500417, -29.50247984919015209, -1.443849546365046699 ) ) ;
#27122=CARTESIAN_POINT ( 'NONE',  ( -16.00611555608923098, 13.71732778110762219, -1.500000000000002220 ) ) ;
#27125=CARTESIAN_POINT ( 'NONE',  ( -48.87380231474225667, -25.25252557466923520, 6.137092008254006359 ) ) ;
#27126=CARTESIAN_POINT ( 'NONE',  ( -120.5173578655454918, -24.73531770709095312, 8.716586749053508498 ) ) ;
#27128=CARTESIAN_POINT ( 'NONE',  ( -76.59214368814321006, -24.15620529776628089, 10.23563542870660470 ) ) ;
#27129=B_SPLINE_CURVE_WITH_KNOTS ( 'NONE', 3,
 ( #40769, #9307, #96552, #32652, #71730, #34168 ),
 .UNSPECIFIED., .F., .F.,
 ( 4, 2, 4 ),
 ( 6.384118678618878472E-06, 0.001386860460828378888, 0.002767336802978138856 ),
 .UNSPECIFIED. ) ;
#27130=CARTESIAN_POINT ( 'NONE',  ( -118.6228709571500559, -24.64965695001469115, 8.947790433994175174 ) ) ;
#27131=CARTESIAN_POINT ( 'NONE',  ( 21.66353188042378974, 1.267531592894010739, -1.500000000000002220 ) ) ;
#27132=CARTESIAN_POINT ( 'NONE',  ( -80.52846833935618065, -25.24759804693422893, 7.100555191934691202 ) ) ;
#27133=CARTESIAN_POINT ( 'NONE',  ( 2.725811458822067657, 22.07344620009914138, 11.49999999999999645 ) ) ;
#27134=ORIENTED_EDGE ( 'NONE', *, *, #49541, .F. ) ;
#27135=ADVANCED_FACE ( 'NONE', ( #27268 ), #81047, .F. ) ;
#27138=DIRECTION ( 'NONE',  ( -3.773278334453079030E-23, 0.9999999999976377785, 2.173523156925979128E-06 ) ) ;
#27140=DIRECTION ( 'NONE',  ( -3.773278334453079618E-23, 0.9999999999976377785, 2.173523156925979975E-06 ) ) ;
#27141=ORIENTED_EDGE ( 'NONE', *, *, #27342, .T. ) ;
#27143=CARTESIAN_POINT ( 'NONE',  ( -95.55620429048339304, -24.99156044556202261, 7.747789690856174083 ) ) ;
#27144=B_SPLINE_CURVE_WITH_KNOTS ( 'NONE', 3,
 ( #53607, #7400, #57606, #48991 ),
 .UNSPECIFIED., .F., .F.,
 ( 4, 4 ),
 ( 0.2689542867207789789, 0.2699550337615441720 ),
 .UNSPECIFIED. ) ;
#27145=CARTESIAN_POINT ( 'NONE',  ( -49.22466177438518287, -25.30474062507557065, 4.482496648232663361 ) ) ;
#27147=CARTESIAN_POINT ( 'NONE',  ( -105.5228709571501184, -24.83602698348160942, 1.605859176311261294 ) ) ;
#27148=VERTEX_POINT ( 'NONE', #32880 ) ;
#27149=CARTESIAN_POINT ( 'NONE',  ( -130.5728709571500872, -25.30388856787854479, 6.584556770830782391 ) ) ;
#27151=CARTESIAN_POINT ( 'NONE',  ( -22.46026885398333661, -0.8929446408661095846, -1.500000000000002220 ) ) ;
#27152=ORIENTED_EDGE ( 'NONE', *, *, #1607, .T. ) ;
#27153=CARTESIAN_POINT ( 'NONE',  ( -81.52287095715007581, -23.73934037231757088, 11.05740245334329153 ) ) ;
#27154=CARTESIAN_POINT ( 'NONE',  ( -101.5089391001824310, -24.66019654487200086, 8.947790411086115725 ) ) ;
#27157=CARTESIAN_POINT ( 'NONE',  ( -125.5228709571500616, -24.83602698348235904, 1.605859176313918946 ) ) ;
#27158=CARTESIAN_POINT ( 'NONE',  ( -130.5728709571501156, -25.30558673197061736, 5.002395802403323266 ) ) ;
#27159=ADVANCED_FACE ( 'NONE', ( #42505 ), #11037, .T. ) ;
#27160=CARTESIAN_POINT ( 'NONE',  ( -7.889300446747370188, -17.95381117360125955, -1.500000000000002220 ) ) ;
#27161=B_SPLINE_SURFACE_WITH_KNOTS ( 'NONE', 3, 3, ( 
 ( #62871, #84674, #91777, #22260 ),
 ( #99879, #53242, #85175, #68461 ),
 ( #15160, #100378, #440, #76056 ),
 ( #29891, #77550, #46127, #16162 ),
 ( #22759, #77053, #31393, #76546 ),
 ( #85682, #30891, #93787, #83674 ),
 ( #46632, #47130, #24283, #7054 ) ),
 .UNSPECIFIED., .F., .F., .F.,
 ( 4, 3, 4 ),
 ( 4, 4 ),
 ( 0.0004766839783820474058, 0.1029713700210894145, 0.2054660560637967814 ),
 ( 0.6796668928939724186, 0.6809932145055455077 ),
 .UNSPECIFIED. ) ;
#27163=ORIENTED_EDGE ( 'NONE', *, *, #77713, .F. ) ;
#27164=CARTESIAN_POINT ( 'NONE',  ( -14.25192491085926072, -16.12266454619898326, 11.49999999999998934 ) ) ;
#27167=CARTESIAN_POINT ( 'NONE',  ( -71.30457154551153565, -25.25639407517100565, 6.209207384461286061 ) ) ;
#27168=CARTESIAN_POINT ( 'NONE',  ( -69.52287095715009002, -23.48783264082477018, -1.443836473390092801 ) ) ;
#27170=CARTESIAN_POINT ( 'NONE',  ( 3.929728083993185184, -22.62717521373229701, -1.500000000000002220 ) ) ;
#27174=CARTESIAN_POINT ( 'NONE',  ( -49.59336093443951654, -24.15543982623906771, -0.2315651400026657036 ) ) ;
#27175=CARTESIAN_POINT ( 'NONE',  ( 19.99232773509726258, 2.034096180923423702, 11.49999999999999645 ) ) ;
#27179=PLANE ( 'NONE',  #5265 ) ;
#27180=CARTESIAN_POINT ( 'NONE',  ( -65.62287095715008434, -24.82558206586145033, 1.605769216559450152 ) ) ;
#27182=CARTESIAN_POINT ( 'NONE',  ( 7.713363164125232707, -18.29545692620113684, -1.500000000000002220 ) ) ;
#27183=B_SPLINE_CURVE_WITH_KNOTS ( 'NONE', 3,
 ( #39809, #92588, #54058, #70266, #93586, #47434 ),
 .UNSPECIFIED., .F., .F.,
 ( 4, 2, 4 ),
 ( 0.000000000000000000, 0.001380901958385389412, 0.002761803916770778824 ),
 .UNSPECIFIED. ) ;
#27184=DIRECTION ( 'NONE',  ( 0.000000000000000000, 0.9999999999976377785, 2.173523156925979975E-06 ) ) ;
#27185=CARTESIAN_POINT ( 'NONE',  ( 8.221391366598689743, 17.94232518691122635, -1.500000000000002220 ) ) ;
#27186=AXIS2_PLACEMENT_3D ( 'NONE', #87301, #34527, #42653 ) ;
#27189=FACE_OUTER_BOUND ( 'NONE', #16083, .T. ) ;
#27191=CARTESIAN_POINT ( 'NONE',  ( -7.658335995763069448, 19.15843701367676388, 11.49999999999999645 ) ) ;
#27195=ADVANCED_FACE ( 'NONE', ( #96769 ), #56233, .F. ) ;
#27196=CARTESIAN_POINT ( 'NONE',  ( 22.15051849217804403, -4.756829024181505439, 11.49999999999999645 ) ) ;
#27197=ORIENTED_EDGE ( 'NONE', *, *, #96739, .F. ) ;
#27198=CARTESIAN_POINT ( 'NONE',  ( -102.5228709571500758, -24.65952944569305316, 1.056160979905702346 ) ) ;
#27199=CARTESIAN_POINT ( 'NONE',  ( -56.52287095715007581, -24.34917612406836795, 0.1852690917426530193 ) ) ;
#27202=CARTESIAN_POINT ( 'NONE',  ( -56.52287095715008292, -24.66019654487199375, 8.947790411086122830 ) ) ;
#27205=VERTEX_POINT ( 'NONE', #41492 ) ;
#27207=CARTESIAN_POINT ( 'NONE',  ( -22.32109313027335062, -5.015931025267754251, -1.500000000000002220 ) ) ;
#27209=CARTESIAN_POINT ( 'NONE',  ( -21.57561264457377348, 0.06291308125064201673, -1.500000000000002220 ) ) ;
#27210=CARTESIAN_POINT ( 'NONE',  ( -113.5528490827367847, -24.35071581493543746, 9.817618358456018157 ) ) ;
#27212=CARTESIAN_POINT ( 'NONE',  ( -6.671648801611133273, 21.52854475820963032, 11.49999999999999645 ) ) ;
#27214=CARTESIAN_POINT ( 'NONE',  ( -43.49940552739553112, -24.15543982623906771, -0.2315651400026568496 ) ) ;
#27215=CARTESIAN_POINT ( 'NONE',  ( 3.092608977599853315, -21.74436839971096802, 11.49999999999998934 ) ) ;
#27216=DIRECTION ( 'NONE',  ( -3.773278334444167608E-23, 1.000000000000000000, 0.000000000000000000 ) ) ;
#27217=CARTESIAN_POINT ( 'NONE',  ( -29.05583327267715532, -25.21724757842646625, 6.516962117439502933 ) ) ;
#27219=B_SPLINE_CURVE_WITH_KNOTS ( 'NONE', 3,
 ( #35542, #21285, #88830, #28913, #11196, #50266 ),
 .UNSPECIFIED., .F., .F.,
 ( 4, 2, 4 ),
 ( 6.391158118963033910E-06, 0.001387004593080781809, 0.002767618028042600261 ),
 .UNSPECIFIED. ) ;
#27220=LINE ( 'NONE', #96718, #68638 ) ;
#27222=ORIENTED_EDGE ( 'NONE', *, *, #92041, .T. ) ;
#27224=CARTESIAN_POINT ( 'NONE',  ( -19.23287947355762384, -7.152392467615741545, -1.500000000000002220 ) ) ;
#27225=ORIENTED_EDGE ( 'NONE', *, *, #19553, .T. ) ;
#27227=ORIENTED_EDGE ( 'NONE', *, *, #75784, .T. ) ;
#27229=CARTESIAN_POINT ( 'NONE',  ( -60.62287095715004881, -25.00158670708908915, 2.256160236439166855 ) ) ;
#27231=CARTESIAN_POINT ( 'NONE',  ( -50.38191529551148307, -25.12049752546737835, 2.832404795212222659 ) ) ;
#27232=CARTESIAN_POINT ( 'NONE',  ( -14.54385459823299875, 14.27422344363935025, -1.500000000000002220 ) ) ;
#27236=CARTESIAN_POINT ( 'NONE',  ( -92.52287095715006160, -23.48786465467241769, 11.44779295918254292 ) ) ;
#27237=DIRECTION ( 'NONE',  ( 3.773278334444166432E-23, -1.000000000000000000, 0.000000000000000000 ) ) ;
#27238=CARTESIAN_POINT ( 'NONE',  ( -71.43409008949743111, -25.25855267881839339, 7.038380820086293177 ) ) ;
#27240=CARTESIAN_POINT ( 'NONE',  ( -76.62287095715007013, -23.47593901973091235, -1.443836447539004642 ) ) ;
#27241=CARTESIAN_POINT ( 'NONE',  ( -94.58953762381672448, -23.47593901973091235, -1.443836447539002865 ) ) ;
#27242=VERTEX_POINT ( 'NONE', #95274 ) ;
#27243=CARTESIAN_POINT ( 'NONE',  ( -15.22196369898608737, 14.14466773073655581, 11.49999999999998934 ) ) ;
#27245=EDGE_LOOP ( 'NONE', ( #86011, #78841, #80765, #60264 ) ) ;
#27246=DIRECTION ( 'NONE',  ( 0.000000000000000000, -2.173523156925980399E-06, 0.9999999999976378895 ) ) ;
#27247=VERTEX_POINT ( 'NONE', #33875 ) ;
#27248=B_SPLINE_SURFACE_WITH_KNOTS ( 'NONE', 3, 3, ( 
 ( #23313, #55799, #7600, #53790 ),
 ( #39052, #54297, #47679, #39558 ),
 ( #31946, #85225, #7101, #61407 ),
 ( #46172, #78594, #23822, #38554 ),
 ( #46677, #70000, #489, #31440 ),
 ( #47178, #78096, #8610, #62917 ),
 ( #93838, #24325, #55298, #9102 ) ),
 .UNSPECIFIED., .F., .F., .F.,
 ( 4, 3, 4 ),
 ( 4, 4 ),
 ( 0.7945040050992236980, 0.8970133687736494554, 0.9995227324480751019 ),
 ( 0.01949895220031790111, 0.02052067876555380838 ),
 .UNSPECIFIED. ) ;
#27249=EDGE_CURVE ( 'NONE', #16063, #79151, #61119, .T. ) ;
#27250=CARTESIAN_POINT ( 'NONE',  ( -41.56944306088920627, -23.48786465467240347, 11.44779295918255002 ) ) ;
#27252=ORIENTED_EDGE ( 'NONE', *, *, #84031, .F. ) ;
#27253=VERTEX_POINT ( 'NONE', #34874 ) ;
#27254=CARTESIAN_POINT ( 'NONE',  ( -112.5562042904833930, -23.48783264082478794, -1.443836473390060604 ) ) ;
#27257=CARTESIAN_POINT ( 'NONE',  ( -70.90175588921343319, -25.24515073813446264, 5.458926565674500964 ) ) ;
#27258=CARTESIAN_POINT ( 'NONE',  ( 21.87352179494074633, -3.179377960941109915, 11.49999999999999645 ) ) ;
#27260=EDGE_CURVE ( 'NONE', #87003, #93974, #46549, .T. ) ;
#27261=CARTESIAN_POINT ( 'NONE',  ( -103.6235449539058919, -24.65952944569304606, 1.056160979905703234 ) ) ;
#27262=CARTESIAN_POINT ( 'NONE',  ( 22.48748499206561746, 2.281147167042596013, -1.500000000000002220 ) ) ;
#27263=AXIS2_PLACEMENT_3D ( 'NONE', #51013, #12433, #75325 ) ;
#27265=CARTESIAN_POINT ( 'NONE',  ( -115.5510435398882692, -24.83644354573579349, 8.397322867130096569 ) ) ;
#27266=ORIENTED_EDGE ( 'NONE', *, *, #93289, .F. ) ;
#27268=FACE_OUTER_BOUND ( 'NONE', #79473, .T. ) ;
#27269=VECTOR ( 'NONE', #3042, 1000.000000000000114 ) ;
#27270=CARTESIAN_POINT ( 'NONE',  ( -57.53372114876139420, -24.66019654487198665, 8.947790411086121054 ) ) ;
#27272=CARTESIAN_POINT ( 'NONE',  ( 3.105769797727405024, 20.95935918496786599, -1.500000000000002220 ) ) ;
#27275=CARTESIAN_POINT ( 'NONE',  ( -41.86233165767207964, -25.29049933140881734, 4.390697414263186715 ) ) ;
#27276=CARTESIAN_POINT ( 'NONE',  ( 21.63714550250683644, -5.416328558471028565, -1.500000000000002220 ) ) ;
#27281=FACE_OUTER_BOUND ( 'NONE', #36213, .T. ) ;
#27284=CARTESIAN_POINT ( 'NONE',  ( -19.34354882100874562, 2.624169249526263403, 11.49999999999998934 ) ) ;
#27285=CARTESIAN_POINT ( 'NONE',  ( -13.24026558610970916, 16.85365899302435722, -1.500000000000002220 ) ) ;
#27286=CARTESIAN_POINT ( 'NONE',  ( -27.70544111104076990, -24.92774666352100965, 1.628749181268301927 ) ) ;
#27287=CARTESIAN_POINT ( 'NONE',  ( -111.5228709571500616, -29.50250243563736774, 8.947779886222136270 ) ) ;
#27288=CARTESIAN_POINT ( 'NONE',  ( -77.50833635574721825, -24.15543982623907482, -0.2315651400026658147 ) ) ;
#27289=CARTESIAN_POINT ( 'NONE',  ( -22.57016884136470125, -3.422276288085174478, -1.500000000000002220 ) ) ;
#27290=EDGE_CURVE ( 'NONE', #45491, #67032, #51404, .T. ) ;
#27291=CARTESIAN_POINT ( 'NONE',  ( -102.6311358316829825, -23.96119346886881729, -0.6495511937831878191 ) ) ;
#27293=CARTESIAN_POINT ( 'NONE',  ( -16.79965634883036074, 10.71410036745690597, 11.49999999999999645 ) ) ;
#27294=CARTESIAN_POINT ( 'NONE',  ( -104.6305873691463404, -23.96119346886880663, -0.6495511937832033622 ) ) ;
#27295=CARTESIAN_POINT ( 'NONE',  ( -39.53917220841552194, -24.35071581493542681, 9.817618358456035921 ) ) ;
#27296=CARTESIAN_POINT ( 'NONE',  ( -48.50071888450607105, -24.15543982623907482, -0.2315651400026527418 ) ) ;
#27299=CARTESIAN_POINT ( 'NONE',  ( -31.23333084502592882, -24.87219037988794312, 1.747789950295619787 ) ) ;
#27300=CARTESIAN_POINT ( 'NONE',  ( 20.80172415560569021, 6.174449132348904357, 11.49999999999998934 ) ) ;
#27301=CARTESIAN_POINT ( 'NONE',  ( -56.51485917416104598, -23.73791477778911840, 11.05961554403170766 ) ) ;
#27302=CARTESIAN_POINT ( 'NONE',  ( 18.95637782189878706, 4.751392969308117387, -1.500000000000002220 ) ) ;
#27303=CARTESIAN_POINT ( 'NONE',  ( -93.52287095715007581, -23.73907113216989018, -1.053371485793250129 ) ) ;
#27306=CARTESIAN_POINT ( 'NONE',  ( -15.55180764702766716, 13.24544322234432414, 11.49999999999999645 ) ) ;
#27307=CARTESIAN_POINT ( 'NONE',  ( -49.44071097719352537, -25.28921703305024948, 5.643882662217386326 ) ) ;
#27308=CARTESIAN_POINT ( 'NONE',  ( -63.62287095715004881, -23.47593901973091235, -1.443836447539007972 ) ) ;
#27311=CARTESIAN_POINT ( 'NONE',  ( -123.6228709571500559, -29.50248528299804818, 1.056150453629045360 ) ) ;
#27312=CARTESIAN_POINT ( 'NONE',  ( -102.6228709571500417, -23.48786465467241769, 11.44779295918253936 ) ) ;
#27317=LINE ( 'NONE', #67386, #88482 ) ;
#27320=ADVANCED_FACE ( 'NONE', ( #21130 ), #67834, .T. ) ;
#27321=CARTESIAN_POINT ( 'NONE',  ( -9.967090755842360039, -20.75144515299163217, 11.49999999999999645 ) ) ;
#27322=CARTESIAN_POINT ( 'NONE',  ( -13.85039312988123150, 18.09399583546626289, -1.500000000000002220 ) ) ;
#27324=CARTESIAN_POINT ( 'NONE',  ( -26.33488822642538452, -29.50249716773871356, 6.524111834107554131 ) ) ;
#27326=EDGE_CURVE ( 'NONE', #18521, #55686, #75411, .T. ) ;
#27327=CARTESIAN_POINT ( 'NONE',  ( -78.52287095715006160, -23.48786465467241769, 11.44779295918254469 ) ) ;
#27328=CARTESIAN_POINT ( 'NONE',  ( -89.52287095715004739, -24.51283580621451819, 0.6167428607046001598 ) ) ;
#27329=CARTESIAN_POINT ( 'NONE',  ( -3.281320334969873631, 21.64054093270537393, 11.49999999999998934 ) ) ;
#27332=DIRECTION ( 'NONE',  ( 1.000000000000000000, 3.773278334444166432E-23, 8.201307841325785021E-29 ) ) ;
#27336=CARTESIAN_POINT ( 'NONE',  ( -1.067026067711715154, -20.38227831319515460, -1.500000000000002220 ) ) ;
#27337=VERTEX_POINT ( 'NONE', #83528 ) ;
#27338=ORIENTED_EDGE ( 'NONE', *, *, #84341, .T. ) ;
#27342=EDGE_CURVE ( 'NONE', #5107, #59954, #12575, .T. ) ;
#27343=CARTESIAN_POINT ( 'NONE',  ( -11.53412672884717871, -19.92380006517282709, 11.49999999999998934 ) ) ;
#27344=FACE_OUTER_BOUND ( 'NONE', #96840, .T. ) ;
#27345=CARTESIAN_POINT ( 'NONE',  ( 14.76687977769557847, -13.71354340032049457, -1.500000000000002220 ) ) ;
#27347=CARTESIAN_POINT ( 'NONE',  ( -97.62287095715007013, -24.34917612406837861, 0.1852690917426668693 ) ) ;
#27349=CARTESIAN_POINT ( 'NONE',  ( -101.5228709571500900, -23.96177878511308634, 10.65340807706329507 ) ) ;
#27351=CARTESIAN_POINT ( 'NONE',  ( 15.73328655151706101, -14.44092690703295467, 11.49999999999999645 ) ) ;
#27352=VERTEX_POINT ( 'NONE', #20635 ) ;
#27353=DIRECTION ( 'NONE',  ( 0.6837766319725330222, 0.000000000000000000, -0.7296913851542302654 ) ) ;
#27354=VERTEX_POINT ( 'NONE', #97270 ) ;
#27355=CARTESIAN_POINT ( 'NONE',  ( 19.22371909900314435, 11.20011194808016342, 11.49999999999998934 ) ) ;
#27356=CARTESIAN_POINT ( 'NONE',  ( 20.01179378540625819, 5.277757631783551950, 11.49999999999998934 ) ) ;
#27357=EDGE_CURVE ( 'NONE', #92089, #17028, #5397, .T. ) ;
#27358=VERTEX_POINT ( 'NONE', #43983 ) ;
#27359=DIRECTION ( 'NONE',  ( -3.773278334453079030E-23, 0.9999999999976377785, 2.173523156925979128E-06 ) ) ;
#27362=EDGE_LOOP ( 'NONE', ( #96479, #81026, #92102, #10092 ) ) ;
#27363=CARTESIAN_POINT ( 'NONE',  ( -50.32469610480872291, -25.10935127440189163, 2.834264403437368962 ) ) ;
#27364=CARTESIAN_POINT ( 'NONE',  ( -18.84683179826791743, -9.195131953753229226, -1.500000000000002220 ) ) ;
#27365=CARTESIAN_POINT ( 'NONE',  ( 15.10893391618534665, -15.86458014800626692, 11.49999999999999645 ) ) ;
#27366=B_SPLINE_CURVE_WITH_KNOTS ( 'NONE', 3,
 ( #36436, #14087, #44556, #37443, #75482, #82608 ),
 .UNSPECIFIED., .F., .F.,
 ( 4, 2, 4 ),
 ( 1.570887131794176733E-05, 0.001396322306279757170, 0.002776935741241572803 ),
 .UNSPECIFIED. ) ;
#27368=CARTESIAN_POINT ( 'NONE',  ( -26.56775203954515874, -24.89279871775309516, 6.997625193822926803 ) ) ;
#27369=CARTESIAN_POINT ( 'NONE',  ( -17.96456891314058879, -13.58578184957126034, -1.500000000000002220 ) ) ;
#27370=CARTESIAN_POINT ( 'NONE',  ( 10.03794737889396771, 18.37758748099471973, -1.500000000000002220 ) ) ;
#27372=CARTESIAN_POINT ( 'NONE',  ( -110.5228709571500474, -24.82558206586148231, 1.605769216559631563 ) ) ;
#27374=B_SPLINE_CURVE_WITH_KNOTS ( 'NONE', 3,
 ( #2968, #97300, #95796, #57266 ),
 .UNSPECIFIED., .F., .F.,
 ( 4, 4 ),
 ( 2.775557561562891043E-17, 9.999999999998898659E-05 ),
 .UNSPECIFIED. ) ;
#27375=CARTESIAN_POINT ( 'NONE',  ( -119.6235012026005080, -24.66019654487200441, 8.947790411086108620 ) ) ;
#27377=ORIENTED_EDGE ( 'NONE', *, *, #91809, .F. ) ;
#27379=VERTEX_POINT ( 'NONE', #30241 ) ;
#27380=EDGE_LOOP ( 'NONE', ( #63194, #99552, #83488, #83244 ) ) ;
#27383=CARTESIAN_POINT ( 'NONE',  ( -8.943896628894790979, 19.53434260886740503, -1.500000000000002220 ) ) ;
#27384=EDGE_CURVE ( 'NONE', #12369, #41069, #77972, .T. ) ;
#27387=CARTESIAN_POINT ( 'NONE',  ( 20.77832821955112408, -3.674247523096572099, 11.49999999999998934 ) ) ;
#27390=VECTOR ( 'NONE', #3764, 1000.000000000000114 ) ;
#27392=CARTESIAN_POINT ( 'NONE',  ( -80.35919894935767616, -25.29534345321060940, 4.505481338261425606 ) ) ;
#27394=CARTESIAN_POINT ( 'NONE',  ( -21.88945651911318535, 3.243594245096953710, -1.500000000000002220 ) ) ;
#27395=VERTEX_POINT ( 'NONE', #45492 ) ;
#27396=CARTESIAN_POINT ( 'NONE',  ( -81.50565816229075722, -24.35071581493543036, 9.817618358456037697 ) ) ;
#27397=CARTESIAN_POINT ( 'NONE',  ( -111.6228709571500559, -29.50250786944525672, 11.44777988621622988 ) ) ;
#27398=CARTESIAN_POINT ( 'NONE',  ( -40.89894032811586300, -25.27956060308583730, 5.492539715312949156 ) ) ;
#27400=CARTESIAN_POINT ( 'NONE',  ( -62.54857352048542651, -24.15620529776627734, 10.23563542870660825 ) ) ;
#27403=CARTESIAN_POINT ( 'NONE',  ( -15.06583839362908961, -15.15408912208086534, -1.500000000000002220 ) ) ;
#27404=CARTESIAN_POINT ( 'NONE',  ( -69.00578779554861342, -25.20549243710579290, 6.637794156083747232 ) ) ;
#27405=CARTESIAN_POINT ( 'NONE',  ( -50.91839352580279865, -25.25978491487771649, 3.590542621692356384 ) ) ;
#27406=CARTESIAN_POINT ( 'NONE',  ( -64.50990493018097993, -23.96169478059713498, 10.65365249895718058 ) ) ;
#27408=CARTESIAN_POINT ( 'NONE',  ( 22.38532167473930556, -2.757513164441831144, -1.500000000000002220 ) ) ;
#27409=B_SPLINE_CURVE_WITH_KNOTS ( 'NONE', 3,
 ( #23136, #62743, #69838, #93657, #8930, #78932 ),
 .UNSPECIFIED., .F., .F.,
 ( 4, 2, 4 ),
 ( 6.391158118958420121E-06, 0.001387004593080778557, 0.002767618028042598960 ),
 .UNSPECIFIED. ) ;
#27411=ORIENTED_EDGE ( 'NONE', *, *, #25017, .T. ) ;
#27412=PLANE ( 'NONE',  #27186 ) ;
#27413=CARTESIAN_POINT ( 'NONE',  ( -79.50500068773956741, -24.34968618360933945, 0.1864209137778814473 ) ) ;
#27414=CARTESIAN_POINT ( 'NONE',  ( 19.48663422773152121, -3.193742178437300794, 11.49999999999999645 ) ) ;
#27416=AXIS2_PLACEMENT_3D ( 'NONE', #61791, #36935, #67906 ) ;
#27417=B_SPLINE_CURVE_WITH_KNOTS ( 'NONE', 3,
 ( #77744, #8259, #78749, #79259 ),
 .UNSPECIFIED., .F., .F.,
 ( 4, 4 ),
 ( 0.6309505463409755821, 0.6399569776130914489 ),
 .UNSPECIFIED. ) ;
#27418=B_SPLINE_CURVE_WITH_KNOTS ( 'NONE', 3,
 ( #82235, #4126, #75120, #12715 ),
 .UNSPECIFIED., .F., .F.,
 ( 4, 4 ),
 ( 0.000000000000000000, 9.999999999998897304E-05 ),
 .UNSPECIFIED. ) ;
#27419=CARTESIAN_POINT ( 'NONE',  ( -32.07722060962684907, -25.33442522607536418, 4.656390931545514533 ) ) ;
#27422=CARTESIAN_POINT ( 'NONE',  ( -29.02540380353726590, -25.26026405050802026, 2.175342404154256837 ) ) ;
#27424=CARTESIAN_POINT ( 'NONE',  ( 11.61936018155104833, -18.21891831228114356, 11.49999999999998934 ) ) ;
#27425=DIRECTION ( 'NONE',  ( -1.000000000000000000, -3.773278334444166432E-23, -8.201307841325785021E-29 ) ) ;
#27428=FACE_OUTER_BOUND ( 'NONE', #42250, .T. ) ;
#27429=CARTESIAN_POINT ( 'NONE',  ( 17.16143643543069075, 9.858047367376444825, -1.500000000000002220 ) ) ;
#27431=CARTESIAN_POINT ( 'NONE',  ( 5.347689060783223702, 19.56899250667117229, 11.49999999999999645 ) ) ;
#27432=CARTESIAN_POINT ( 'NONE',  ( -54.62287095715005592, -24.66019654487199020, 8.947790411086135265 ) ) ;
#27433=AXIS2_PLACEMENT_3D ( 'NONE', #82448, #91555, #36782 ) ;
#27437=B_SPLINE_SURFACE_WITH_KNOTS ( 'NONE', 3, 3, ( 
 ( #90844, #21315, #89845, #96459 ),
 ( #4118, #5606, #52286, #81734 ),
 ( #11224, #58417, #42202, #5106 ),
 ( #50299, #4620, #73133, #65541 ) ),
 .UNSPECIFIED., .F., .F., .F.,
 ( 4, 4 ),
 ( 4, 4 ),
 ( 0.5133787333263793995, 0.6547335371774368751 ),
 ( 0.7903368604290639254, 0.8131061223386927272 ),
 .UNSPECIFIED. ) ;
#27438=CARTESIAN_POINT ( 'NONE',  ( -99.52925925567853938, -25.26679311647689730, 4.031539577752753623 ) ) ;
#27440=CARTESIAN_POINT ( 'NONE',  ( -71.52287095715010423, -24.66019654487200086, 8.947790411086115725 ) ) ;
#27442=CARTESIAN_POINT ( 'NONE',  ( -52.52287095715006870, -24.64898659630367916, 1.056161002820821038 ) ) ;
#27443=ADVANCED_FACE ( 'NONE', ( #39362 ), #22616, .T. ) ;
#27445=CARTESIAN_POINT ( 'NONE',  ( 4.692034869050136336, 19.47840706813412126, -1.500000000000002220 ) ) ;
#27446=EDGE_CURVE ( 'NONE', #67691, #54301, #77903, .T. ) ;
#27448=ORIENTED_EDGE ( 'NONE', *, *, #8647, .F. ) ;
#27451=LINE ( 'NONE', #35060, #50220 ) ;
#27454=B_SPLINE_CURVE_WITH_KNOTS ( 'NONE', 3,
 ( #68646, #69133, #38679, #100055, #84855, #7225 ),
 .UNSPECIFIED., .F., .F.,
 ( 4, 2, 4 ),
 ( 0.000000000000000000, 0.001380764517854768869, 0.002761529035709537738 ),
 .UNSPECIFIED. ) ;
#27457=FACE_OUTER_BOUND ( 'NONE', #56827, .T. ) ;
#27458=ORIENTED_EDGE ( 'NONE', *, *, #38257, .F. ) ;
#27460=CARTESIAN_POINT ( 'NONE',  ( -20.32193514540556123, 0.06534614623005505218, 11.49999999999998934 ) ) ;
#27463=CARTESIAN_POINT ( 'NONE',  ( 0.5590224530292132732, -22.91010021869659852, -1.500000000000002220 ) ) ;
#27464=CARTESIAN_POINT ( 'NONE',  ( -32.56126115692759981, -23.73766607897670866, -1.055555164236441801 ) ) ;
#27467=CARTESIAN_POINT ( 'NONE',  ( -37.62287095715005592, -23.72747288104441665, -1.053458166803663110 ) ) ;
#27468=CARTESIAN_POINT ( 'NONE',  ( -50.36234373730416536, -25.26264178341608968, 7.100826787533305762 ) ) ;
#27470=AXIS2_PLACEMENT_3D ( 'NONE', #3750, #89473, #19948 ) ;
#27472=CARTESIAN_POINT ( 'NONE',  ( -20.81765089029956783, 3.879123387127271005, 11.49999999999999645 ) ) ;
#27473=CARTESIAN_POINT ( 'NONE',  ( -12.03526013704878039, -18.61824004984164560, -1.500000000000002220 ) ) ;
#27474=CARTESIAN_POINT ( 'NONE',  ( 19.36870410414886479, 7.000668502413378569, 11.49999999999998934 ) ) ;
#27477=CARTESIAN_POINT ( 'NONE',  ( -41.62876366737128819, -24.51314013834315375, 0.6176544820404115121 ) ) ;
#27478=EDGE_LOOP ( 'NONE', ( #20746, #75875, #31457, #31770 ) ) ;
#27480=CARTESIAN_POINT ( 'NONE',  ( -49.62287095715005592, -24.64898659630528499, 1.056161002820821038 ) ) ;
#27481=ORIENTED_EDGE ( 'NONE', *, *, #2145, .T. ) ;
#27482=ORIENTED_EDGE ( 'NONE', *, *, #98325, .F. ) ;
#27483=ORIENTED_EDGE ( 'NONE', *, *, #91269, .T. ) ;
#27484=CARTESIAN_POINT ( 'NONE',  ( -77.52287095715006160, -24.66019654487200086, 8.947790411086113949 ) ) ;
#27485=CARTESIAN_POINT ( 'NONE',  ( -71.62287095715005592, -24.64965695001468404, 8.947790433994184056 ) ) ;
#27486=CARTESIAN_POINT ( 'NONE',  ( -102.5228709571500758, -24.64965694238407323, 8.947790433994194714 ) ) ;
#27487=CARTESIAN_POINT ( 'NONE',  ( 5.171613189315443115, 20.13430294385436881, -1.500000000000002220 ) ) ;
#27488=CARTESIAN_POINT ( 'NONE',  ( 16.47784684176308545, -14.13017478139203220, 11.49999999999999645 ) ) ;
#27491=CARTESIAN_POINT ( 'NONE',  ( -96.52287095715006160, -24.65952944569304606, 1.056160979905702346 ) ) ;
#27492=CARTESIAN_POINT ( 'NONE',  ( 6.649717926671450563, 21.43536518531312396, 11.49999999999998934 ) ) ;
#27495=CARTESIAN_POINT ( 'NONE',  ( -65.61529522140628501, -23.48783264082477018, -1.443836473390096353 ) ) ;
#27497=CARTESIAN_POINT ( 'NONE',  ( -83.62287095715005592, -24.64965695001468404, 8.947790433994182280 ) ) ;
#27498=CARTESIAN_POINT ( 'NONE',  ( -119.4728709571500502, -25.40674640480649416, 5.000950437805936843 ) ) ;
#27499=B_SPLINE_CURVE_WITH_KNOTS ( 'NONE', 3,
 ( #81254, #11736, #27969, #97959 ),
 .UNSPECIFIED., .F., .F.,
 ( 4, 4 ),
 ( 0.000000000000000000, 1.000000000000000000 ),
 .UNSPECIFIED. ) ;
#27500=ORIENTED_EDGE ( 'NONE', *, *, #71911, .F. ) ;
#27501=ORIENTED_EDGE ( 'NONE', *, *, #43043, .T. ) ;
#27502=EDGE_CURVE ( 'NONE', #37803, #19978, #44025, .T. ) ;
#27503=CARTESIAN_POINT ( 'NONE',  ( -69.62287095715004170, -23.96177878511307568, 10.65340807706330395 ) ) ;
#27504=ORIENTED_EDGE ( 'NONE', *, *, #23937, .F. ) ;
#27506=CARTESIAN_POINT ( 'NONE',  ( -12.43717309395686499, -17.31322327496724611, -1.500000000000002220 ) ) ;
#27509=CARTESIAN_POINT ( 'NONE',  ( -6.661741538832703036, 20.79550341630197607, -1.500000000000002220 ) ) ;
#27511=CARTESIAN_POINT ( 'NONE',  ( 7.379361219544559702, 21.46082085352547963, 11.49999999999998934 ) ) ;
#27512=CARTESIAN_POINT ( 'NONE',  ( -41.39385049892748469, -25.28892541658160553, 3.844044583132800064 ) ) ;
#27513=DIRECTION ( 'NONE',  ( -1.000000000000000000, -3.773278334444167608E-23, -8.201307833595939069E-29 ) ) ;
#27514=CARTESIAN_POINT ( 'NONE',  ( -4.809782828112996178, 21.40371668077904488, -1.500000000000002220 ) ) ;
#27515=CARTESIAN_POINT ( 'NONE',  ( -68.52287095715006160, -29.50248528299804818, 1.056150453629036701 ) ) ;
#27517=CARTESIAN_POINT ( 'NONE',  ( -122.5889729151568162, -24.51419770103158413, 9.386484678747169852 ) ) ;
#27518=CARTESIAN_POINT ( 'NONE',  ( -115.6228709571500701, -25.00158670708909625, 2.256160236439165967 ) ) ;
#27519=ORIENTED_EDGE ( 'NONE', *, *, #86430, .F. ) ;
#27522=CARTESIAN_POINT ( 'NONE',  ( -88.52287095715009002, -24.66019654487200441, 8.947790411086119278 ) ) ;
#27523=CARTESIAN_POINT ( 'NONE',  ( -10.25207789694340299, -22.90580643265542093, 0.5637492489085903502 ) ) ;
#27524=CARTESIAN_POINT ( 'NONE',  ( -21.26230640008892792, -0.7210608269398429693, 11.49999999999998934 ) ) ;
#27525=CARTESIAN_POINT ( 'NONE',  ( -55.62287095715006302, -24.63345952396254646, 9.038047939301511846 ) ) ;
#27526=CARTESIAN_POINT ( 'NONE',  ( -107.6228709571500701, -23.47596703998600631, 11.44779298504227860 ) ) ;
#27528=CARTESIAN_POINT ( 'NONE',  ( -85.54116237476874574, -24.83618233451451118, 1.606449574219533272 ) ) ;
#27529=CARTESIAN_POINT ( 'NONE',  ( -68.51066526543451118, -23.96119346886880663, -0.6495511937832112448 ) ) ;
#27530=CARTESIAN_POINT ( 'NONE',  ( -39.62287095715006302, -23.73934037231756378, 11.05740245334329863 ) ) ;
#27532=CARTESIAN_POINT ( 'NONE',  ( 19.54226456527178257, 0.3027743077981833730, 11.49999999999999645 ) ) ;
#27533=CARTESIAN_POINT ( 'NONE',  ( -43.22287095715006444, -23.47593901973090169, -1.443836447538997980 ) ) ;
#27537=VERTEX_POINT ( 'NONE', #6909 ) ;
#27538=CARTESIAN_POINT ( 'NONE',  ( -117.5228709571500758, -23.72773821059536914, 11.05748984161097326 ) ) ;
#27539=CARTESIAN_POINT ( 'NONE',  ( -99.22760414877923552, -25.31352189248182682, 5.229817175528475026 ) ) ;
#27543=CARTESIAN_POINT ( 'NONE',  ( 19.18734209777730015, 4.435579877058994036, -1.500000000000002220 ) ) ;
#27545=ORIENTED_EDGE ( 'NONE', *, *, #46132, .F. ) ;
#27550=EDGE_CURVE ( 'NONE', #5356, #3446, #13818, .T. ) ;
#27554=DIRECTION ( 'NONE',  ( -3.773278334444167608E-23, 1.000000000000000000, 0.000000000000000000 ) ) ;
#27555=CARTESIAN_POINT ( 'NONE',  ( -55.52200631800427999, -23.48783264082475952, -1.443836473390099462 ) ) ;
#27556=CARTESIAN_POINT ( 'NONE',  ( -118.5885976234968808, -24.51314013834317151, 0.6176544820404233915 ) ) ;
#27558=EDGE_CURVE ( 'NONE', #59306, #36357, #27144, .T. ) ;
#27561=CARTESIAN_POINT ( 'NONE',  ( -12.66726347749767179, -15.43046242340049545, -1.500000000000002220 ) ) ;
#27563=CARTESIAN_POINT ( 'NONE',  ( -0.04267401778350129321, -22.49755130481472420, 8.628546368132811395 ) ) ;
#27564=CARTESIAN_POINT ( 'NONE',  ( -8.676013072486071565, -17.92234406281952275, -1.500000000000002220 ) ) ;
#27566=CARTESIAN_POINT ( 'NONE',  ( -63.52287095715004739, -23.94994826722563985, -0.6494450866342731388 ) ) ;
#27568=EDGE_CURVE ( 'NONE', #42765, #54649, #68297, .T. ) ;
#27571=CARTESIAN_POINT ( 'NONE',  ( -49.62287095715005592, -24.66019654487199020, 8.947790411086135265 ) ) ;
#27577=PLANE ( 'NONE',  #1546 ) ;
#27579=CARTESIAN_POINT ( 'NONE',  ( -13.58233929615340152, 14.99024694321910900, 11.49999999999998934 ) ) ;
#27583=B_SPLINE_CURVE_WITH_KNOTS ( 'NONE', 3,
 ( #72234, #18436, #81835, #81338, #10324, #50397, #27055, #11820 ),
 .UNSPECIFIED., .F., .F.,
 ( 4, 2, 2, 4 ),
 ( 0.000000000000000000, 0.002001098010032686687, 0.003001647015049031548, 0.004002196020065376843 ),
 .UNSPECIFIED. ) ;
#27584=ORIENTED_EDGE ( 'NONE', *, *, #9007, .T. ) ;
#27585=CARTESIAN_POINT ( 'NONE',  ( -80.15869489321136143, -25.31558262175477481, 4.989020118345524502 ) ) ;
#27587=CARTESIAN_POINT ( 'NONE',  ( 4.397486433803790007, -19.56896378179033036, -1.500000000000002220 ) ) ;
#27588=CARTESIAN_POINT ( 'NONE',  ( -11.62490142266122639, -17.50836435561060256, 11.49999999999999645 ) ) ;
#27590=CARTESIAN_POINT ( 'NONE',  ( -70.54092792707334070, -24.63419186844611986, 9.035850630976923981 ) ) ;
#27591=CARTESIAN_POINT ( 'NONE',  ( 18.88560736741940005, 11.47387103136259690, -1.500000000000002220 ) ) ;
#27593=CARTESIAN_POINT ( 'NONE',  ( -39.48225211724125927, -25.31589192678097433, 4.451013730343944985 ) ) ;
#27595=PLANE ( 'NONE',  #76797 ) ;
#27597=CARTESIAN_POINT ( 'NONE',  ( -72.51141342689224700, -23.96119346886880663, -0.6495511937832121330 ) ) ;
#27600=B_SPLINE_CURVE_WITH_KNOTS ( 'NONE', 3,
 ( #57891, #41155, #72108, #26426 ),
 .UNSPECIFIED., .F., .F.,
 ( 4, 4 ),
 ( 0.000000000000000000, 1.000000000000000000 ),
 .UNSPECIFIED. ) ;
#27603=CARTESIAN_POINT ( 'NONE',  ( -43.22287095715006444, -23.47596703998600276, 11.44779298504227683 ) ) ;
#27604=CARTESIAN_POINT ( 'NONE',  ( -125.2228709571500644, -23.47596703998600631, 11.44779298504227860 ) ) ;
#27606=CARTESIAN_POINT ( 'NONE',  ( 1.511266892140219920, 20.53031905857337591, -1.500000000000002220 ) ) ;
#27607=CARTESIAN_POINT ( 'NONE',  ( -4.138935798035190849, -21.16376344109877294, 11.49999999999999645 ) ) ;
#27610=LINE ( 'NONE', #36215, #22309 ) ;
#27611=CARTESIAN_POINT ( 'NONE',  ( -97.58953762381672448, -23.48783264082478794, -1.443836473390061936 ) ) ;
#27612=CARTESIAN_POINT ( 'NONE',  ( -11.77839732991513166, 18.97803183815481987, 11.49999999999998934 ) ) ;
#27613=DIRECTION ( 'NONE',  ( -3.773278334453079618E-23, 0.9999999999976377785, 2.173523156925979975E-06 ) ) ;
#27614=DIRECTION ( 'NONE',  ( 0.000000000000000000, -0.9999999999976377785, -2.173523156925979975E-06 ) ) ;
#27615=ORIENTED_EDGE ( 'NONE', *, *, #64244, .F. ) ;
#27616=LINE ( 'NONE', #74767, #17757 ) ;
#27617=CARTESIAN_POINT ( 'NONE',  ( -96.58953762381672448, -23.48786465467241413, 11.44779295918254114 ) ) ;
#27618=AXIS2_PLACEMENT_3D ( 'NONE', #88751, #50186, #42583 ) ;
#27619=CARTESIAN_POINT ( 'NONE',  ( 19.90007246472742608, 6.374896562862660154, -1.500000000000002220 ) ) ;
#27620=VERTEX_POINT ( 'NONE', #40863 ) ;
#27623=ORIENTED_EDGE ( 'NONE', *, *, #48393, .F. ) ;
#27625=AXIS2_PLACEMENT_3D ( 'NONE', #98772, #90672, #53127 ) ;
#27626=CARTESIAN_POINT ( 'NONE',  ( -100.5075804452173571, -24.73531770709095312, 8.716586749053508498 ) ) ;
#27627=CARTESIAN_POINT ( 'NONE',  ( -20.44436638909326120, 5.324712401148210539, -1.500000000000002220 ) ) ;
#27630=CARTESIAN_POINT ( 'NONE',  ( -28.52287095715005094, -24.34106804586823714, 0.6165375242712651804 ) ) ;
#27632=DIRECTION ( 'NONE',  ( -3.773278334453079618E-23, 0.9999999999976377785, 2.173523156925979975E-06 ) ) ;
#27635=CARTESIAN_POINT ( 'NONE',  ( 19.97611268498323511, -8.487024919450899318, -1.500000000000002220 ) ) ;
#27636=CARTESIAN_POINT ( 'NONE',  ( -80.48900664166535535, -25.24759804928183726, 7.101635288197144291 ) ) ;
#27637=CARTESIAN_POINT ( 'NONE',  ( 15.88595335714125589, -15.59144682577495189, 11.49999999999999645 ) ) ;
#27639=CARTESIAN_POINT ( 'NONE',  ( -77.22287095715009286, -23.47593901973090524, -1.443836447538997980 ) ) ;
#27641=CARTESIAN_POINT ( 'NONE',  ( -50.40445135320379677, -25.12298712672050982, 7.101635559041870494 ) ) ;
#27642=ORIENTED_EDGE ( 'NONE', *, *, #60014, .T. ) ;
#27644=VERTEX_POINT ( 'NONE', #26137 ) ;
#27646=CARTESIAN_POINT ( 'NONE',  ( -0.1426030150137701236, -21.20389190742571373, -1.497999999999532594 ) ) ;
#27647=DIRECTION ( 'NONE',  ( 0.000000000000000000, -2.173523156925979552E-06, 0.9999999999976378895 ) ) ;
#27650=CARTESIAN_POINT ( 'NONE',  ( -107.5228709571501042, -23.48783264083360578, -1.443836473376361118 ) ) ;
#27651=PLANE ( 'NONE',  #70074 ) ;
#27653=CARTESIAN_POINT ( 'NONE',  ( 0.06232057257353295493, 19.38168652127415825, 11.49999999999999645 ) ) ;
#27655=CARTESIAN_POINT ( 'NONE',  ( 3.503984654965784706, -22.18958196551723816, -1.500000000000002220 ) ) ;
#27659=B_SPLINE_CURVE_WITH_KNOTS ( 'NONE', 3,
 ( #62122, #32151, #78318, #14922, #77807, #54010 ),
 .UNSPECIFIED., .F., .F.,
 ( 4, 2, 4 ),
 ( 1.570887131794333942E-05, 0.001396322306279757387, 0.002776935741241571502 ),
 .UNSPECIFIED. ) ;
#27661=CARTESIAN_POINT ( 'NONE',  ( -97.24679249956406579, -24.75179208683297460, 8.640809912072082710 ) ) ;
#27662=CARTESIAN_POINT ( 'NONE',  ( 19.39309126630920588, -2.812899550206792831, -1.500000000000002220 ) ) ;
#27663=CARTESIAN_POINT ( 'NONE',  ( -46.48372047104909655, -24.65952944569304606, 1.056160979905696351 ) ) ;
#27664=ORIENTED_EDGE ( 'NONE', *, *, #97905, .T. ) ;
#27665=CARTESIAN_POINT ( 'NONE',  ( -2.508422780830330989, 21.39056295969660582, -1.500000000000002220 ) ) ;
#27666=LINE ( 'NONE', #33775, #57713 ) ;
#27667=CARTESIAN_POINT ( 'NONE',  ( -81.37613735670856840, -25.30394805385784807, 5.179459886602215235 ) ) ;
#27668=CARTESIAN_POINT ( 'NONE',  ( -62.55620429048337883, -24.64965694238574656, 8.947790433994198267 ) ) ;
#27671=CARTESIAN_POINT ( 'NONE',  ( 22.09143763772896918, 6.410036269187016522, -1.500000000000002220 ) ) ;
#27673=CARTESIAN_POINT ( 'NONE',  ( -93.62287095715005592, -24.66019654487199730, 8.947790411086124607 ) ) ;
#27674=CARTESIAN_POINT ( 'NONE',  ( -79.62287095715005592, -24.64898659630528854, 1.056161002820826145 ) ) ;
#27675=CARTESIAN_POINT ( 'NONE',  ( -17.52916707085001136, 9.785066945116392745, 11.49999999999999645 ) ) ;
#27676=CARTESIAN_POINT ( 'NONE',  ( -109.6441887128288784, -25.10927429713856540, 2.986266705731216664 ) ) ;
#27677=CARTESIAN_POINT ( 'NONE',  ( -32.49648798523244153, -24.15620529776627734, 10.23563542870661358 ) ) ;
#27679=CARTESIAN_POINT ( 'NONE',  ( -90.62287095715004170, -29.50250786944525672, 11.44777988621623344 ) ) ;
#27680=CARTESIAN_POINT ( 'NONE',  ( -100.4498239493576648, -25.03284467579916495, 7.563174216508126158 ) ) ;
#27681=CARTESIAN_POINT ( 'NONE',  ( 6.283368587668265448, -18.83516890145298106, 11.49999999999998934 ) ) ;
#27683=CARTESIAN_POINT ( 'NONE',  ( -113.5508063869240658, -24.65952944569304606, 1.056160979905704789 ) ) ;
#27684=CARTESIAN_POINT ( 'NONE',  ( 11.88433821776028942, -15.71472908967258242, -1.500000000000002220 ) ) ;
#27685=CARTESIAN_POINT ( 'NONE',  ( -42.53415887033509790, -24.51314013834315375, 0.6176544820404090697 ) ) ;
#27688=EDGE_CURVE ( 'NONE', #71376, #35617, #72322, .T. ) ;
#27692=CARTESIAN_POINT ( 'NONE',  ( 18.87225196054570020, 8.368929400942139551, 11.49999999999999645 ) ) ;
#27694=CARTESIAN_POINT ( 'NONE',  ( -128.5228709571501042, -24.51387760970726504, 9.387446482453400520 ) ) ;
#27695=CARTESIAN_POINT ( 'NONE',  ( 19.67839991682829748, -11.23141783594569354, 11.49999999999999645 ) ) ;
#27696=ORIENTED_EDGE ( 'NONE', *, *, #6248, .T. ) ;
#27700=DIRECTION ( 'NONE',  ( -3.773278334453079618E-23, 0.9999999999976377785, 2.173523156925979975E-06 ) ) ;
#27702=EDGE_LOOP ( 'NONE', ( #12373, #87545, #69258, #79578 ) ) ;
#27703=EDGE_LOOP ( 'NONE', ( #5628, #33746, #40206, #78734 ) ) ;
#27704=CARTESIAN_POINT ( 'NONE',  ( -49.62287095715005592, -29.50247984919015209, -1.443849546365058689 ) ) ;
#27705=CARTESIAN_POINT ( 'NONE',  ( -1.055347110731411187, -22.84297022578905612, 11.49999999999998934 ) ) ;
#27707=CARTESIAN_POINT ( 'NONE',  ( 19.98343133220876666, -8.209121646405339590, -1.500000000000002220 ) ) ;
#27708=CARTESIAN_POINT ( 'NONE',  ( -113.5541376391153960, -24.15620529776628800, 10.23563542870659582 ) ) ;
#27709=DIRECTION ( 'NONE',  ( 0.000000000000000000, -0.9999999999976377785, -2.173523156925979128E-06 ) ) ;
#27710=CARTESIAN_POINT ( 'NONE',  ( 19.88857169258762170, 10.62688394266798930, 11.49999999999999645 ) ) ;
#27713=CARTESIAN_POINT ( 'NONE',  ( 21.30657626330824783, 5.479626006175059239, 11.49999999999998934 ) ) ;
#27714=CARTESIAN_POINT ( 'NONE',  ( -111.5512764650698614, -24.51314013834316796, 0.6176544820404207270 ) ) ;
#27715=PLANE ( 'NONE',  #31429 ) ;
#27716=ORIENTED_EDGE ( 'NONE', *, *, #53860, .F. ) ;
#27717=CARTESIAN_POINT ( 'NONE',  ( -89.62287095715004170, -24.66019654487199020, 8.947790411086128159 ) ) ;
#27721=ORIENTED_EDGE ( 'NONE', *, *, #97384, .T. ) ;
#27723=VERTEX_POINT ( 'NONE', #81431 ) ;
#27725=DIRECTION ( 'NONE',  ( -3.773278334453080206E-23, 0.9999999999976377785, 2.173523156925979975E-06 ) ) ;
#27726=CARTESIAN_POINT ( 'NONE',  ( -57.62367078942418885, -24.65952944569304606, 1.056160979905698571 ) ) ;
#27727=CARTESIAN_POINT ( 'NONE',  ( 1.124825640313904973, 20.40429917142216354, -1.500000000000002220 ) ) ;
#27728=ORIENTED_EDGE ( 'NONE', *, *, #13386, .F. ) ;
#27730=CARTESIAN_POINT ( 'NONE',  ( -51.15652172324698910, -25.15690241117504655, 3.041046503643967114 ) ) ;
#27731=EDGE_CURVE ( 'NONE', #78484, #64607, #66727, .T. ) ;
#27732=CARTESIAN_POINT ( 'NONE',  ( -105.5110145565341924, -24.63355581998386867, 0.9682620441943899925 ) ) ;
#27734=VERTEX_POINT ( 'NONE', #60103 ) ;
#27735=CARTESIAN_POINT ( 'NONE',  ( -27.75618988833547718, -25.21531659070602771, 2.278559006348844118 ) ) ;
#27736=CARTESIAN_POINT ( 'NONE',  ( -27.75512851621423138, -24.63646064523983981, 8.250987297651915853 ) ) ;
#27737=ORIENTED_EDGE ( 'NONE', *, *, #92274, .F. ) ;
#27738=CARTESIAN_POINT ( 'NONE',  ( -18.43438512255917772, -9.567967903218889347, -1.500000000000002220 ) ) ;
#27739=ORIENTED_EDGE ( 'NONE', *, *, #91919, .F. ) ;
#27741=DIRECTION ( 'NONE',  ( 1.000000000000000000, 3.773278334444166432E-23, 8.201307841325785021E-29 ) ) ;
#27742=VERTEX_POINT ( 'NONE', #82414 ) ;
#27744=CARTESIAN_POINT ( 'NONE',  ( -51.59601236526418688, -25.30186097039144499, 5.321576288067153548 ) ) ;
#27745=VERTEX_POINT ( 'NONE', #35261 ) ;
#27747=CARTESIAN_POINT ( 'NONE',  ( -33.52287095715006870, -23.95044443724991368, 10.65354141964649948 ) ) ;
#27750=CARTESIAN_POINT ( 'NONE',  ( -43.64074078125805300, -24.15620529776627379, 10.23563542870661180 ) ) ;
#27751=CARTESIAN_POINT ( 'NONE',  ( 10.71795340210964120, -19.33932934982082585, 11.49999999999999645 ) ) ;
#27754=CARTESIAN_POINT ( 'NONE',  ( 19.13181028273733375, 12.02906595412573232, -1.500000000000002220 ) ) ;
#27755=CARTESIAN_POINT ( 'NONE',  ( -115.5500777739175788, -25.00182538069147142, 7.747789668545041586 ) ) ;
#27758=ORIENTED_EDGE ( 'NONE', *, *, #5898, .T. ) ;
#27760=CARTESIAN_POINT ( 'NONE',  ( -78.52287095715004739, -24.66019654487199375, 8.947790411086119278 ) ) ;
#27762=CARTESIAN_POINT ( 'NONE',  ( -78.62287095715007013, -23.72773821059535848, 11.05748984161097503 ) ) ;
#27763=ORIENTED_EDGE ( 'NONE', *, *, #79480, .F. ) ;
#27764=CARTESIAN_POINT ( 'NONE',  ( -12.03079493616482765, -17.41531974249929249, -1.500000000000002220 ) ) ;
#27767=CARTESIAN_POINT ( 'NONE',  ( 15.82088602905085750, -15.72875506571707760, -1.500000000000002220 ) ) ;
#27769=VERTEX_POINT ( 'NONE', #75295 ) ;
#27771=CARTESIAN_POINT ( 'NONE',  ( -29.52287095715006160, -24.56627961951908645, 8.947790480023282811 ) ) ;
#27772=EDGE_CURVE ( 'NONE', #60342, #33324, #41515, .T. ) ;
#27775=CARTESIAN_POINT ( 'NONE',  ( 14.32981562401322506, -13.22600733894156200, 11.49999999999998934 ) ) ;
#27776=CARTESIAN_POINT ( 'NONE',  ( 18.57079561221590325, -10.74342183689097574, 11.49999999999998934 ) ) ;
#27777=CARTESIAN_POINT ( 'NONE',  ( -27.65533724976895869, -24.57999497193509342, 1.629628004430854871 ) ) ;
#27778=DIRECTION ( 'NONE',  ( 0.000000000000000000, 0.9999999999976377785, 2.173523156925979975E-06 ) ) ;
#27780=CARTESIAN_POINT ( 'NONE',  ( 22.53581206741051446, 3.480912172000575122, -1.500000000000002220 ) ) ;
#27781=B_SPLINE_CURVE_WITH_KNOTS ( 'NONE', 3,
 ( #82941, #51516, #60635, #44404 ),
 .UNSPECIFIED., .F., .F.,
 ( 4, 4 ),
 ( 1.387778780781445521E-17, 9.999999999997510880E-05 ),
 .UNSPECIFIED. ) ;
#27783=FACE_OUTER_BOUND ( 'NONE', #50321, .T. ) ;
#27785=CARTESIAN_POINT ( 'NONE',  ( 15.68239283413728735, 12.23493734220040530, 11.49999999999999645 ) ) ;
#27786=CARTESIAN_POINT ( 'NONE',  ( -104.5222000018547988, -23.48783264082477373, -1.443836473390085695 ) ) ;
#27787=LINE ( 'NONE', #18670, #81400 ) ;
#27788=CARTESIAN_POINT ( 'NONE',  ( -98.62287095715005592, -23.47593901973091235, -1.443836447539001089 ) ) ;
#27790=VERTEX_POINT ( 'NONE', #36252 ) ;
#27792=LINE ( 'NONE', #88703, #23156 ) ;
#27793=CARTESIAN_POINT ( 'NONE',  ( 12.82194709444435077, -17.51738216156474337, -1.500000000000002220 ) ) ;
#27795=CARTESIAN_POINT ( 'NONE',  ( 0.4223197742854877812, 19.52780805513575402, -1.500000000000002220 ) ) ;
#27796=CARTESIAN_POINT ( 'NONE',  ( -55.61923469880454718, -23.48786465467241058, 11.44779295918254647 ) ) ;
#27799=EDGE_CURVE ( 'NONE', #24634, #79371, #75457, .T. ) ;
#27800=CARTESIAN_POINT ( 'NONE',  ( -81.52287095715006160, -24.64965694238408034, 8.947790433994198267 ) ) ;
#27801=CARTESIAN_POINT ( 'NONE',  ( 19.09590870110849181, 7.302211495713927469, 11.49999999999999645 ) ) ;
#27802=CARTESIAN_POINT ( 'NONE',  ( -47.52287095715006870, -23.96177878511308634, 10.65340807706330573 ) ) ;
#27803=AXIS2_PLACEMENT_3D ( 'NONE', #7436, #59751, #60253 ) ;
#27804=EDGE_CURVE ( 'NONE', #14758, #48827, #72971, .T. ) ;
#27805=CARTESIAN_POINT ( 'NONE',  ( -93.52287095715006160, -29.50250243563736774, 8.947779886222139822 ) ) ;
#27806=VERTEX_POINT ( 'NONE', #90526 ) ;
#27807=CARTESIAN_POINT ( 'NONE',  ( -55.58953762381673158, -23.48786465467240703, 11.44779295918255180 ) ) ;
#27808=CARTESIAN_POINT ( 'NONE',  ( -43.52287095715007581, -24.66019654487199375, 8.947790411086128159 ) ) ;
#27810=B_SPLINE_CURVE_WITH_KNOTS ( 'NONE', 3,
 ( #12206, #88349, #42197, #4115, #95956, #27946, #19322, #97454 ),
 .UNSPECIFIED., .F., .F.,
 ( 4, 2, 2, 4 ),
 ( -0.001240666984355833250, -0.0002401179793394929429, 0.0007604310256768473646, 0.002761529035709531232 ),
 .UNSPECIFIED. ) ;
#27811=EDGE_CURVE ( 'NONE', #67935, #48203, #95958, .T. ) ;
#27815=VECTOR ( 'NONE', #55271, 1000.000000000000114 ) ;
#27816=CARTESIAN_POINT ( 'NONE',  ( -4.971178678486217528, -22.47594730032828281, 11.49999999999999645 ) ) ;
#27817=CARTESIAN_POINT ( 'NONE',  ( 0.8422786845129024424, 22.77647355728978340, -1.500000000000002220 ) ) ;
#27819=CARTESIAN_POINT ( 'NONE',  ( -122.5562042904833930, -24.64898659630528854, 1.056161002820831474 ) ) ;
#27820=CARTESIAN_POINT ( 'NONE',  ( -49.72668233141190797, -25.22502443621784707, 3.520239836515675513 ) ) ;
#27822=CARTESIAN_POINT ( 'NONE',  ( -53.22287095715007865, -23.47593901973090169, -1.443836447538997758 ) ) ;
#27823=CARTESIAN_POINT ( 'NONE',  ( -44.58953762381671737, -23.48783264082478084, -1.443836473390072150 ) ) ;
#27824=B_SPLINE_CURVE_WITH_KNOTS ( 'NONE', 3,
 ( #29736, #60704, #91625, #22108, #30734, #53090 ),
 .UNSPECIFIED., .F., .F.,
 ( 4, 2, 4 ),
 ( 1.570887131794176733E-05, 0.001396322306279759555, 0.002776935741241577573 ),
 .UNSPECIFIED. ) ;
#27825=CARTESIAN_POINT ( 'NONE',  ( -19.20277006422315225, 10.48866939257135833, -1.500000000000002220 ) ) ;
#27826=CARTESIAN_POINT ( 'NONE',  ( -59.55620429048336462, -24.64965694238574301, 8.947790433994201820 ) ) ;
#27829=CARTESIAN_POINT ( 'NONE',  ( -96.52287095715006160, -24.64965694238575011, 8.947790433994194714 ) ) ;
#27830=ORIENTED_EDGE ( 'NONE', *, *, #7617, .T. ) ;
#27831=CARTESIAN_POINT ( 'NONE',  ( -13.80512455850298714, -15.04058748057734896, -1.500000000000002220 ) ) ;
#27833=ORIENTED_EDGE ( 'NONE', *, *, #14986, .F. ) ;
#27836=CARTESIAN_POINT ( 'NONE',  ( 23.03040035405544472, 1.057182387018521963, 11.49999999999998934 ) ) ;
#27838=CARTESIAN_POINT ( 'NONE',  ( 18.08294815051442583, 9.098846914115775064, -1.500000000000002220 ) ) ;
#27839=ORIENTED_EDGE ( 'NONE', *, *, #4372, .F. ) ;
#27840=DIRECTION ( 'NONE',  ( 0.000000000000000000, -0.9999999999976377785, -2.173523156925979975E-06 ) ) ;
#27841=CARTESIAN_POINT ( 'NONE',  ( -62.62287095715004881, -29.50250243563736774, 8.947779886222145151 ) ) ;
#27844=CARTESIAN_POINT ( 'NONE',  ( 21.32124590881793225, -1.116183810207903804, 11.49999999999999645 ) ) ;
#27845=ORIENTED_EDGE ( 'NONE', *, *, #95007, .T. ) ;
#27846=CARTESIAN_POINT ( 'NONE',  ( -91.62287095715004170, -29.50247984919015209, -1.443849546365051806 ) ) ;
#27848=CARTESIAN_POINT ( 'NONE',  ( -20.07822104958740539, -9.643837532803976487, 11.49999999999998934 ) ) ;
#27849=CARTESIAN_POINT ( 'NONE',  ( -17.42616458466809704, -11.11377323884725321, 11.49999999999998934 ) ) ;
#27850=ORIENTED_EDGE ( 'NONE', *, *, #75789, .F. ) ;
#27854=ORIENTED_EDGE ( 'NONE', *, *, #21970, .T. ) ;
#27858=CARTESIAN_POINT ( 'NONE',  ( -11.35812032211249090, 17.58211214940072864, -1.500000000000002220 ) ) ;
#27859=B_SPLINE_CURVE_WITH_KNOTS ( 'NONE', 3,
 ( #51754, #13167, #28905, #52253 ),
 .UNSPECIFIED., .F., .F.,
 ( 4, 4 ),
 ( 0.000000000000000000, 9.999999999998897304E-05 ),
 .UNSPECIFIED. ) ;
#27860=CARTESIAN_POINT ( 'NONE',  ( -20.57654891367511851, 7.437132321665034240, 11.49999999999999645 ) ) ;
#27861=CARTESIAN_POINT ( 'NONE',  ( -73.51656078076787537, -23.73791477778911840, 11.05961554403170766 ) ) ;
#27862=CARTESIAN_POINT ( 'NONE',  ( -21.16606679798846358, 7.723709098063864076, 11.49999999999998934 ) ) ;
#27863=CARTESIAN_POINT ( 'NONE',  ( 19.44712688777480736, 7.780496645421295376, -1.500000000000002220 ) ) ;
#27864=CARTESIAN_POINT ( 'NONE',  ( -91.52287095715006160, -23.47593901973090524, -1.443836447538996648 ) ) ;
#27866=CARTESIAN_POINT ( 'NONE',  ( -119.5880674028319959, -24.66019654487200441, 8.947790411086108620 ) ) ;
#27867=CARTESIAN_POINT ( 'NONE',  ( -126.6228709571500843, -24.66019654487200441, 8.947790411086119278 ) ) ;
#27869=B_SPLINE_CURVE_WITH_KNOTS ( 'NONE', 3,
 ( #53007, #52500, #82930, #68223 ),
 .UNSPECIFIED., .F., .F.,
 ( 4, 4 ),
 ( 0.8503931694243046513, 0.8593996006964206291 ),
 .UNSPECIFIED. ) ;
#27870=ORIENTED_EDGE ( 'NONE', *, *, #16116, .F. ) ;
#27873=CARTESIAN_POINT ( 'NONE',  ( -66.62364616943149542, -24.65952944569304250, 1.056160979905692798 ) ) ;
#27875=CARTESIAN_POINT ( 'NONE',  ( 11.41860910855227829, 18.14899599152127152, -1.500000000000002220 ) ) ;
#27877=VERTEX_POINT ( 'NONE', #29126 ) ;
#27878=CARTESIAN_POINT ( 'NONE',  ( 16.98782256641479904, -12.52229676876588371, -1.500000000000002220 ) ) ;
#27885=CARTESIAN_POINT ( 'NONE',  ( -18.17467834739497690, 12.62983929299386965, -1.500000000000002220 ) ) ;
#27886=CARTESIAN_POINT ( 'NONE',  ( -116.5166246991671386, -24.51314013834316086, 0.6176544820404277214 ) ) ;
#27887=CARTESIAN_POINT ( 'NONE',  ( -109.4424681886586228, -25.30227564393651818, 5.310848485335579738 ) ) ;
#27889=EDGE_CURVE ( 'NONE', #72799, #46688, #68105, .T. ) ;
#27890=EDGE_CURVE ( 'NONE', #47659, #55720, #97221, .T. ) ;
#27891=LINE ( 'NONE', #51233, #36613 ) ;
#27895=CARTESIAN_POINT ( 'NONE',  ( 19.36035776617087123, -9.008237321879198234, -1.500000000000002220 ) ) ;
#27896=CARTESIAN_POINT ( 'NONE',  ( -26.19073949106259391, -24.93562033171584957, 6.009727169100417044 ) ) ;
#27897=CARTESIAN_POINT ( 'NONE',  ( -90.70924515653385356, -25.26266127311081888, 3.981777872396910389 ) ) ;
#27898=CARTESIAN_POINT ( 'NONE',  ( -64.60342376047213975, -23.73791477778911840, 11.05961554403170766 ) ) ;
#27899=CARTESIAN_POINT ( 'NONE',  ( -81.39459688428541995, -25.20426285083167173, 6.569653346528638416 ) ) ;
#27900=CARTESIAN_POINT ( 'NONE',  ( 11.26306171725914851, -19.60737681494043727, -1.500000000000002220 ) ) ;
#27901=B_SPLINE_CURVE_WITH_KNOTS ( 'NONE', 3,
 ( #63856, #95279, #70443, #25765, #24260, #33370 ),
 .UNSPECIFIED., .F., .F.,
 ( 4, 2, 4 ),
 ( 1.570755371633856203E-05, 0.001396183895866087319, 0.002776660238015836012 ),
 .UNSPECIFIED. ) ;
#27902=VERTEX_POINT ( 'NONE', #29624 ) ;
#27903=B_SPLINE_CURVE_WITH_KNOTS ( 'NONE', 3,
 ( #27110, #48957, #11382, #49967 ),
 .UNSPECIFIED., .F., .F.,
 ( 4, 4 ),
 ( 0.000000000000000000, 0.001261718750000008493 ),
 .UNSPECIFIED. ) ;
#27905=CARTESIAN_POINT ( 'NONE',  ( -79.56369746381113828, -23.48783264082476308, -1.443836473390096575 ) ) ;
#27906=CARTESIAN_POINT ( 'NONE',  ( 9.261118129494249729, -17.44851725036260248, 11.49999999999999645 ) ) ;
#27907=CARTESIAN_POINT ( 'NONE',  ( -74.62287095715005592, -23.48783264082478794, -1.443836473390067265 ) ) ;
#27908=CARTESIAN_POINT ( 'NONE',  ( -47.62287095715004881, -24.64898659630367916, 1.056161002820821038 ) ) ;
#27910=VERTEX_POINT ( 'NONE', #8286 ) ;
#27911=DIRECTION ( 'NONE',  ( -1.000000000000000000, -3.773278334444167608E-23, -8.201307833595939069E-29 ) ) ;
#27912=CARTESIAN_POINT ( 'NONE',  ( -29.81001385051325414, -24.60094546151839623, 4.645691122018320129 ) ) ;
#27914=CARTESIAN_POINT ( 'NONE',  ( -21.09935167195790839, -4.734744157926700225, 11.49999999999998934 ) ) ;
#27915=LINE ( 'NONE', #52753, #51232 ) ;
#27916=CARTESIAN_POINT ( 'NONE',  ( 2.021814659504407579E-13, -19.30000000000000426, -1.500000000000002220 ) ) ;
#27917=CARTESIAN_POINT ( 'NONE',  ( -109.6228709571500559, -23.47593901973091235, -1.443836447538999312 ) ) ;
#27918=DIRECTION ( 'NONE',  ( -3.773278334444167608E-23, 1.000000000000000000, 0.000000000000000000 ) ) ;
#27919=CARTESIAN_POINT ( 'NONE',  ( -6.431973572030615038, 18.70533856667250916, -1.500000000000002220 ) ) ;
#27920=ORIENTED_EDGE ( 'NONE', *, *, #14792, .F. ) ;
#27921=CARTESIAN_POINT ( 'NONE',  ( 15.52975653788041122, 12.98207780544785628, 11.49999999999999645 ) ) ;
#27922=CARTESIAN_POINT ( 'NONE',  ( -54.52287095715005449, -24.66019654487198665, 8.947790411086121054 ) ) ;
#27923=B_SPLINE_CURVE_WITH_KNOTS ( 'NONE', 3,
 ( #60887, #77581, #86212, #7585, #91816, #23803 ),
 .UNSPECIFIED., .F., .F.,
 ( 4, 2, 4 ),
 ( 0.000000000000000000, 0.001380901958385387894, 0.002761803916770775788 ),
 .UNSPECIFIED. ) ;
#27924=EDGE_CURVE ( 'NONE', #85301, #39996, #87518, .T. ) ;
#27925=DIRECTION ( 'NONE',  ( 0.000000000000000000, 2.173523156925980399E-06, -0.9999999999976378895 ) ) ;
#27926=AXIS2_PLACEMENT_3D ( 'NONE', #73939, #87159, #48619 ) ;
#27929=CARTESIAN_POINT ( 'NONE',  ( -110.5895376238167103, -24.99132157543166954, 2.256160258750667502 ) ) ;
#27931=CARTESIAN_POINT ( 'NONE',  ( -75.58953762381673869, -23.48783264082478084, -1.443836473390065489 ) ) ;
#27933=CARTESIAN_POINT ( 'NONE',  ( -51.39961447129974204, -25.19579413596467177, 6.633757500754181358 ) ) ;
#27934=CARTESIAN_POINT ( 'NONE',  ( 3.179702300980958185, 19.78100630842630281, -1.500000000000002220 ) ) ;
#27936=FACE_OUTER_BOUND ( 'NONE', #67071, .T. ) ;
#27939=B_SPLINE_CURVE_WITH_KNOTS ( 'NONE', 3,
 ( #24772, #55754, #77553, #61363 ),
 .UNSPECIFIED., .F., .F.,
 ( 4, 4 ),
 ( 0.000000000000000000, 9.999999999999592548E-05 ),
 .UNSPECIFIED. ) ;
#27940=EDGE_CURVE ( 'NONE', #48556, #45754, #10059, .T. ) ;
#27941=CARTESIAN_POINT ( 'NONE',  ( -73.62287095715004170, -23.72773821059535848, 11.05748984161097681 ) ) ;
#27943=CARTESIAN_POINT ( 'NONE',  ( -117.5228709571500758, -24.64965694238408034, 8.947790433994191162 ) ) ;
#27944=CARTESIAN_POINT ( 'NONE',  ( -84.62287095715005592, -23.47593901973091235, -1.443836447539004642 ) ) ;
#27945=AXIS2_PLACEMENT_3D ( 'NONE', #18203, #63908, #57291 ) ;
#27946=CARTESIAN_POINT ( 'NONE',  ( -105.5228709571500474, -24.14321612903114200, -0.2833117244521580758 ) ) ;
#27947=DIRECTION ( 'NONE',  ( -3.773278334453080206E-23, 0.9999999999976377785, 2.173523156925979975E-06 ) ) ;
#27950=CARTESIAN_POINT ( 'NONE',  ( 18.28078834835902455, 8.925752885971231620, -1.500000000000002220 ) ) ;
#27952=CARTESIAN_POINT ( 'NONE',  ( 9.743704349311032686, 20.77413290702584092, -1.500000000000002220 ) ) ;
#27953=CARTESIAN_POINT ( 'NONE',  ( -32.48286750831535841, -24.51314013834315375, 0.6176544820404111791 ) ) ;
#27954=ORIENTED_EDGE ( 'NONE', *, *, #18529, .F. ) ;
#27955=CARTESIAN_POINT ( 'NONE',  ( -50.40895856474225667, -25.03284467579915784, 7.563174216508125269 ) ) ;
#27959=CARTESIAN_POINT ( 'NONE',  ( -17.86006801910157193, 11.38285951858322242, 11.49999999999999645 ) ) ;
#27960=ORIENTED_EDGE ( 'NONE', *, *, #45465, .F. ) ;
#27963=CARTESIAN_POINT ( 'NONE',  ( -2.513997614918375589, -22.02279109229760223, -1.500000000000002220 ) ) ;
#27964=CARTESIAN_POINT ( 'NONE',  ( 19.85042311639309531, 5.490197614093233369, -1.500000000000002220 ) ) ;
#27966=VECTOR ( 'NONE', #56632, 1000.000000000000114 ) ;
#27967=ORIENTED_EDGE ( 'NONE', *, *, #35921, .T. ) ;
#27969=CARTESIAN_POINT ( 'NONE',  ( -77.58953762381673869, -23.47593901973091235, -1.443836447539004642 ) ) ;
#27972=ORIENTED_EDGE ( 'NONE', *, *, #85738, .T. ) ;
#27973=AXIS2_PLACEMENT_3D ( 'NONE', #45220, #60949, #22349 ) ;
#27974=CARTESIAN_POINT ( 'NONE',  ( -77.52287095715009002, -23.96177878511308990, 10.65340807706329684 ) ) ;
#27975=B_SPLINE_CURVE_WITH_KNOTS ( 'NONE', 3,
 ( #3914, #58196, #19113, #43956 ),
 .UNSPECIFIED., .F., .F.,
 ( 4, 4 ),
 ( 0.5902073771187474893, 0.5992138083908630231 ),
 .UNSPECIFIED. ) ;
#27976=CARTESIAN_POINT ( 'NONE',  ( -108.6228709571500417, -24.65952944569305316, 1.056160979905705011 ) ) ;
#27977=DIRECTION ( 'NONE',  ( -3.773278334453080206E-23, 0.9999999999976377785, 2.173523156925979975E-06 ) ) ;
#27978=CARTESIAN_POINT ( 'NONE',  ( -15.76495264167062160, -13.51897010167481739, -1.500000000000002220 ) ) ;
#27979=CARTESIAN_POINT ( 'NONE',  ( 21.56942612084361599, 2.798134137018522427, 11.49999999999999645 ) ) ;
#27980=VERTEX_POINT ( 'NONE', #23487 ) ;
#27981=CARTESIAN_POINT ( 'NONE',  ( -40.45829750704998418, -25.18492896333868103, 3.293943116708551777 ) ) ;
#27982=CARTESIAN_POINT ( 'NONE',  ( -37.58953762381673158, -24.66019654487199375, 8.947790411086137041 ) ) ;
#27983=DIRECTION ( 'NONE',  ( -3.773278334453079618E-23, 0.9999999999976377785, 2.173523156925979975E-06 ) ) ;
#27984=CARTESIAN_POINT ( 'NONE',  ( 15.48037617655995923, 16.25473645317415361, -1.500000000000002220 ) ) ;
#27986=CARTESIAN_POINT ( 'NONE',  ( -124.5228709571500332, -23.73934037231757443, 11.05740245334327732 ) ) ;
#27987=ORIENTED_EDGE ( 'NONE', *, *, #23694, .T. ) ;
#27988=DIRECTION ( 'NONE',  ( 0.000000000000000000, 2.173523156925979975E-06, -0.9999999999976378895 ) ) ;
#27989=CARTESIAN_POINT ( 'NONE',  ( -89.67764846858844408, -25.05712135967895549, 7.447789548357304668 ) ) ;
#27990=B_SPLINE_SURFACE_WITH_KNOTS ( 'NONE', 3, 3, ( 
 ( #22076, #20589, #30195, #82983 ),
 ( #51561, #22565, #99690, #6372 ),
 ( #37332, #76363, #44445, #29706 ),
 ( #91103, #92099, #53060, #52551 ),
 ( #90607, #82490, #83484, #12974 ),
 ( #28716, #44948, #29211, #43939 ),
 ( #74872, #14467, #36329, #59677 ),
 ( #67794, #84488, #13475, #98712 ),
 ( #75372, #45449, #5375, #67287 ),
 ( #6866, #61177, #60179, #21088 ) ),
 .UNSPECIFIED., .F., .F., .F.,
 ( 4, 3, 3, 4 ),
 ( 4, 4 ),
 ( 0.7022005934544807149, 0.7765311282028797280, 0.8508616629512786300, 0.9995227324480764342 ),
 ( 0.3995422158643850974, 0.4007930624188544289 ),
 .UNSPECIFIED. ) ;
#27991=ORIENTED_EDGE ( 'NONE', *, *, #67338, .F. ) ;
#27992=ORIENTED_EDGE ( 'NONE', *, *, #55449, .F. ) ;
#27993=CARTESIAN_POINT ( 'NONE',  ( -87.62287095715004170, -23.47593901973091235, -1.443836447539002865 ) ) ;
#27996=EDGE_CURVE ( 'NONE', #28945, #50965, #63268, .T. ) ;
#27997=CARTESIAN_POINT ( 'NONE',  ( -18.83571791729191958, -9.990160686573538840, -1.500000000000002220 ) ) ;
#28000=CARTESIAN_POINT ( 'NONE',  ( 13.86046232669119149, 16.88393516940953276, -1.500000000000002220 ) ) ;
#28001=CARTESIAN_POINT ( 'NONE',  ( -55.55620429048340014, -23.47596703998600276, 11.44779298504227505 ) ) ;
#28002=CARTESIAN_POINT ( 'NONE',  ( 17.32531159343115945, 14.66459048539768162, -1.500000000000002220 ) ) ;
#28003=CARTESIAN_POINT ( 'NONE',  ( -40.93315603532715130, -25.18430893389220060, 3.395436753013815423 ) ) ;
#28004=CARTESIAN_POINT ( 'NONE',  ( -124.5228709571500616, -23.47593901973090524, -1.443836447538996204 ) ) ;
#28005=CARTESIAN_POINT ( 'NONE',  ( -20.07106029494397248, -8.819774368769808248, -1.500000000000002220 ) ) ;
#28006=CARTESIAN_POINT ( 'NONE',  ( -109.5228709571500474, -24.66019654487200086, 8.947790411086119278 ) ) ;
#28008=CARTESIAN_POINT ( 'NONE',  ( -122.5195445546590918, -24.35071581493544102, 9.817618358456019934 ) ) ;
#28010=AXIS2_PLACEMENT_3D ( 'NONE', #46427, #7860, #23572 ) ;
#28013=ORIENTED_EDGE ( 'NONE', *, *, #3162, .T. ) ;
#28015=CARTESIAN_POINT ( 'NONE',  ( -30.61237075433887966, -24.38737281877371643, 9.682478639550817334 ) ) ;
#28020=CARTESIAN_POINT ( 'NONE',  ( 16.87399902462237478, -12.92443306546820736, 11.49999999999998934 ) ) ;
#28021=CARTESIAN_POINT ( 'NONE',  ( -110.5228709571500616, -29.50250786944525672, 11.44777988621622988 ) ) ;
#28023=CARTESIAN_POINT ( 'NONE',  ( -114.5228709571500616, -23.48783264083396105, -1.443836473375806895 ) ) ;
#28024=FACE_OUTER_BOUND ( 'NONE', #79225, .T. ) ;
#28027=CARTESIAN_POINT ( 'NONE',  ( -19.49195742049215241, -1.735909528584683947, 11.49999999999999645 ) ) ;
#28028=CARTESIAN_POINT ( 'NONE',  ( -78.52287095715006160, -23.73934037231757088, 11.05740245334328975 ) ) ;
#28029=CARTESIAN_POINT ( 'NONE',  ( -28.16520605572959468, -24.69042538764675143, 8.198497088267734156 ) ) ;
#28031=ORIENTED_EDGE ( 'NONE', *, *, #2432, .F. ) ;
#28033=CARTESIAN_POINT ( 'NONE',  ( -44.55620429048338593, -24.65952944569303895, 1.056160979905692576 ) ) ;
#28036=CARTESIAN_POINT ( 'NONE',  ( -41.62287095715006302, -24.64898659630367561, 1.056161002820819261 ) ) ;
#28037=CARTESIAN_POINT ( 'NONE',  ( 17.66836560233463516, 8.693963128369697202, 11.49999999999998934 ) ) ;
#28038=EDGE_CURVE ( 'NONE', #6656, #2820, #86251, .T. ) ;
#28041=DIRECTION ( 'NONE',  ( -3.773278334453079618E-23, 0.9999999999976377785, 2.173523156925979975E-06 ) ) ;
#28043=EDGE_CURVE ( 'NONE', #2872, #62364, #91097, .T. ) ;
#28046=VERTEX_POINT ( 'NONE', #79793 ) ;
#28047=DIRECTION ( 'NONE',  ( -3.773278334453079618E-23, 0.9999999999976377785, 2.173523156925979975E-06 ) ) ;
#28049=CARTESIAN_POINT ( 'NONE',  ( -47.62840667103132830, -24.51314013834316086, 0.6176544820404172853 ) ) ;
#28050=CARTESIAN_POINT ( 'NONE',  ( -118.5222382821682174, -23.48783264082477018, -1.443836473390085695 ) ) ;
#28051=CARTESIAN_POINT ( 'NONE',  ( -49.58953762381672448, -24.64965694238575011, 8.947790433994205372 ) ) ;
#28052=CARTESIAN_POINT ( 'NONE',  ( -70.32437837831572836, -25.24515042352634708, 5.314180867886988402 ) ) ;
#28053=VECTOR ( 'NONE', #83660, 1000.000000000000114 ) ;
#28054=CARTESIAN_POINT ( 'NONE',  ( -85.52287095715004739, -25.00158670708909625, 2.256160236439166411 ) ) ;
#28055=CARTESIAN_POINT ( 'NONE',  ( 4.608267332293128682, -19.41724391825443874, -1.500000000000002220 ) ) ;
#28057=CARTESIAN_POINT ( 'NONE',  ( -0.08004075721539863353, -22.01380949857533409, 0.03441076822783003392 ) ) ;
#28058=ORIENTED_EDGE ( 'NONE', *, *, #35675, .T. ) ;
#28059=CARTESIAN_POINT ( 'NONE',  ( -116.5562042904833788, -23.47596703998600631, 11.44779298504227683 ) ) ;
#28061=B_SPLINE_CURVE_WITH_KNOTS ( 'NONE', 3,
 ( #60359, #22253, #36999, #67963, #98890, #29383 ),
 .UNSPECIFIED., .F., .F.,
 ( 4, 2, 4 ),
 ( 0.000000000000000000, 0.001380764517854764315, 0.002761529035709528630 ),
 .UNSPECIFIED. ) ;
#28065=DIRECTION ( 'NONE',  ( 0.000000000000000000, 0.9999999999976377785, 2.173523156925979975E-06 ) ) ;
#28066=DIRECTION ( 'NONE',  ( 3.773278334444167608E-23, -1.000000000000000000, 0.000000000000000000 ) ) ;
#28068=CARTESIAN_POINT ( 'NONE',  ( -26.50076437627408765, -24.83282267876757743, 2.987432207970394327 ) ) ;
#28071=B_SPLINE_SURFACE_WITH_KNOTS ( 'NONE', 3, 1, ( 
 ( #76356, #67281 ),
 ( #98199, #81993 ),
 ( #59670, #43446 ),
 ( #90600, #52046 ),
 ( #36820, #21571 ),
 ( #97218, #12477 ),
 ( #74376, #35821 ),
 ( #31186, #39804 ),
 ( #14962, #46923 ),
 ( #7347, #46421 ),
 ( #47427, #22559 ),
 ( #70259, #54050 ),
 ( #24571, #23062 ),
 ( #93082, #55548 ),
 ( #38302, #16964 ),
 ( #63159, #30188 ),
 ( #99684, #31695 ),
 ( #77352, #93578 ),
 ( #7854, #39303 ) ),
 .UNSPECIFIED., .F., .F., .F.,
 ( 4, 1, 1, 1, 1, 1, 1, 1, 1, 1, 1, 1, 1, 1, 1, 1, 4 ),
 ( 2, 2 ),
 ( 0.000000000000000000, 0.06523080374203335530, 0.1284048960032229403, 0.1900670715964798418, 0.2509433657682823560, 0.3115458328521446552, 0.3728628021568331508, 0.4350236738562400229, 0.4990717247070452500, 0.5630910750496653794, 0.6255101063303781794, 0.6866800359296505452, 0.7472825030135124003, 0.8085634952159601596, 0.8707421035159864653, 0.9343409515059127868, 1.000000000000000000 ),
 ( 0.000000000000000000, 1.000000000000000000 ),
 .UNSPECIFIED. ) ;
#28072=DIRECTION ( 'NONE',  ( -0.000000000000000000, 2.173523156925979552E-06, -0.9999999999976378895 ) ) ;
#28073=CARTESIAN_POINT ( 'NONE',  ( -127.6242800499748853, -23.96119346886880663, -0.6495511937832001426 ) ) ;
#28074=ORIENTED_EDGE ( 'NONE', *, *, #9626, .F. ) ;
#28075=CARTESIAN_POINT ( 'NONE',  ( 16.63042848490962555, -11.55671354112608817, 11.49999999999998934 ) ) ;
#28076=CARTESIAN_POINT ( 'NONE',  ( -68.93918693012690824, -25.25799956426409665, 6.184868438663939649 ) ) ;
#28077=DIRECTION ( 'NONE',  ( -1.000000000000000000, -3.773278334444166432E-23, -8.201307841325785021E-29 ) ) ;
#28080=ORIENTED_EDGE ( 'NONE', *, *, #63033, .T. ) ;
#28081=CARTESIAN_POINT ( 'NONE',  ( -78.94968344233984681, -25.29062087922736524, 5.787134492223548143 ) ) ;
#28082=CARTESIAN_POINT ( 'NONE',  ( -52.52287095715006870, -23.48786465467241058, 11.44779295918255002 ) ) ;
#28083=CARTESIAN_POINT ( 'NONE',  ( 4.692034869050136336, 19.47840706813412126, -1.500000000000002220 ) ) ;
#28085=CARTESIAN_POINT ( 'NONE',  ( 18.24537196375281312, 10.48796402029766739, 11.49999999999999645 ) ) ;
#28087=CARTESIAN_POINT ( 'NONE',  ( -89.81226385320383088, -25.31788500672307052, 4.644766330052804371 ) ) ;
#28088=CARTESIAN_POINT ( 'NONE',  ( -2.767897998228395551, 21.91458177938747909, -1.500000000000002220 ) ) ;
#28089=CARTESIAN_POINT ( 'NONE',  ( -40.02212956655154130, -25.27806092693242945, 5.017934196670617020 ) ) ;
#28090=CARTESIAN_POINT ( 'NONE',  ( -76.55620429048340725, -23.47593901973091235, -1.443836447539004642 ) ) ;
#28093=CARTESIAN_POINT ( 'NONE',  ( -99.17126091090496232, -25.24403727686683396, 3.682577372028675633 ) ) ;
#28094=CARTESIAN_POINT ( 'NONE',  ( -31.61989000895333746, -23.48783264082477018, -1.443836473390079256 ) ) ;
#28096=VERTEX_POINT ( 'NONE', #72703 ) ;
#28097=CARTESIAN_POINT ( 'NONE',  ( -80.64675904551151575, -25.20074414427590881, 3.409327697718777195 ) ) ;
#28098=FACE_OUTER_BOUND ( 'NONE', #89959, .T. ) ;
#28099=DIRECTION ( 'NONE',  ( 0.000000000000000000, 0.9999999999976377785, 2.173523156925979128E-06 ) ) ;
#28100=CARTESIAN_POINT ( 'NONE',  ( -14.18348626307465743, -14.89297910716571849, -1.500000000000002220 ) ) ;
#28101=CARTESIAN_POINT ( 'NONE',  ( -17.67581969798968444, -12.36387604476075097, 11.49999999999999645 ) ) ;
#28102=ORIENTED_EDGE ( 'NONE', *, *, #29511, .F. ) ;
#28103=CARTESIAN_POINT ( 'NONE',  ( -91.51836583836262662, -23.73766607897670156, -1.055555164236454235 ) ) ;
#28104=LINE ( 'NONE', #43336, #17469 ) ;
#28106=CARTESIAN_POINT ( 'NONE',  ( 9.556255610625576935, 20.19728179944524271, -1.500000000000002220 ) ) ;
#28109=CARTESIAN_POINT ( 'NONE',  ( -98.52287095715006160, -24.64898659630368272, 1.056161002820829697 ) ) ;
#28110=ORIENTED_EDGE ( 'NONE', *, *, #74440, .F. ) ;
#28112=CARTESIAN_POINT ( 'NONE',  ( -51.13317816230360791, -25.30518297057644617, 4.892016129566734151 ) ) ;
#28113=CARTESIAN_POINT ( 'NONE',  ( -0.8937202392249329330, 20.86669477224961256, 11.49999999999998934 ) ) ;
#28115=CARTESIAN_POINT ( 'NONE',  ( -92.52287095715006160, -24.65952944569304606, 1.056160979905700570 ) ) ;
#28116=EDGE_LOOP ( 'NONE', ( #10534, #21229, #25629, #87361 ) ) ;
#28117=VERTEX_POINT ( 'NONE', #16389 ) ;
#28118=AXIS2_PLACEMENT_3D ( 'NONE', #95070, #17439, #41284 ) ;
#28119=CARTESIAN_POINT ( 'NONE',  ( -100.6266774032520601, -24.73531770709095312, 8.716586749053508498 ) ) ;
#28120=CARTESIAN_POINT ( 'NONE',  ( 13.25904570721172604, 16.46799385432867169, -1.500000000000002220 ) ) ;
#28122=CARTESIAN_POINT ( 'NONE',  ( -91.58953762381672448, -24.66019654487198665, 8.947790411086135265 ) ) ;
#28123=CARTESIAN_POINT ( 'NONE',  ( -102.6228709571500559, -23.47596703998600631, 11.44779298504227683 ) ) ;
#28124=EDGE_CURVE ( 'NONE', #28719, #85754, #93608, .T. ) ;
#28125=CARTESIAN_POINT ( 'NONE',  ( -120.5579446662922862, -23.48786465467241769, 11.44779295918253936 ) ) ;
#28126=VECTOR ( 'NONE', #45737, 1000.000000000000114 ) ;
#28128=LINE ( 'NONE', #97624, #51812 ) ;
#28130=CARTESIAN_POINT ( 'NONE',  ( -4.706806674773570620, -21.25045708977441450, -1.500000000000002220 ) ) ;
#28131=CARTESIAN_POINT ( 'NONE',  ( -81.14265914342044539, -25.12224344358931205, 6.882252752011148722 ) ) ;
#28132=CARTESIAN_POINT ( 'NONE',  ( 22.30035941410032763, -0.3387204123245128873, 11.49999999999999645 ) ) ;
#28134=CARTESIAN_POINT ( 'NONE',  ( -45.62287095715005592, -24.52232992886361984, 0.6492154411906032596 ) ) ;
#28135=CARTESIAN_POINT ( 'NONE',  ( -110.3139465455115271, -25.12049752546738191, 2.832404795212222659 ) ) ;
#28136=FACE_OUTER_BOUND ( 'NONE', #99481, .T. ) ;
#28138=ADVANCED_FACE ( 'NONE', ( #70688 ), #26409, .T. ) ;
#28141=ORIENTED_EDGE ( 'NONE', *, *, #40966, .F. ) ;
#28145=LINE ( 'NONE', #44872, #84239 ) ;
#28146=CARTESIAN_POINT ( 'NONE',  ( -76.52287095715007581, -24.64898659630528854, 1.056161002820826145 ) ) ;
#28148=DIRECTION ( 'NONE',  ( -1.000000000000000000, -3.773278334444167608E-23, -8.201307833595939069E-29 ) ) ;
#28149=ORIENTED_EDGE ( 'NONE', *, *, #37785, .F. ) ;
#28150=CARTESIAN_POINT ( 'NONE',  ( 17.07123823605233781, 9.195568589125342029, 11.49999999999999645 ) ) ;
#28151=CARTESIAN_POINT ( 'NONE',  ( -115.5228709571500758, -25.00182538069145721, 7.747789668545101094 ) ) ;
#28152=VERTEX_POINT ( 'NONE', #35137 ) ;
#28156=CARTESIAN_POINT ( 'NONE',  ( -111.7814946224345789, -29.50249240399202222, 4.332395270848422797 ) ) ;
#28158=CARTESIAN_POINT ( 'NONE',  ( 13.97609912898263573, 13.72534901313461653, -1.500000000000002220 ) ) ;
#28159=VECTOR ( 'NONE', #62348, 1000.000000000000114 ) ;
#28161=ORIENTED_EDGE ( 'NONE', *, *, #15046, .T. ) ;
#28162=CARTESIAN_POINT ( 'NONE',  ( 16.61460563260716583, 13.71664681387569118, 11.49999999999998934 ) ) ;
#28163=CARTESIAN_POINT ( 'NONE',  ( -33.58056022833496712, -24.51419770103157347, 9.386484678747185839 ) ) ;
#28164=CARTESIAN_POINT ( 'NONE',  ( -123.6228709571500559, -23.48786465467241769, 11.44779295918253759 ) ) ;
#28165=CARTESIAN_POINT ( 'NONE',  ( -72.62287095715005592, -24.66019654487199020, 8.947790411086131712 ) ) ;
#28166=CARTESIAN_POINT ( 'NONE',  ( -100.4326965455115044, -25.27473221600376618, 3.293942921519102729 ) ) ;
#28167=CARTESIAN_POINT ( 'NONE',  ( 8.869223403490039459, -21.23658630136709391, -1.500000000000002220 ) ) ;
#28170=CARTESIAN_POINT ( 'NONE',  ( -53.58246871847038051, -24.51314013834315730, 0.6176544820404108460 ) ) ;
#28171=CARTESIAN_POINT ( 'NONE',  ( -20.16912494768211417, -0.3064379698199363733, 11.49999999999999645 ) ) ;
#28176=CARTESIAN_POINT ( 'NONE',  ( -122.5228709571500616, -23.48786465467241769, 11.44779295918253759 ) ) ;
#28177=CARTESIAN_POINT ( 'NONE',  ( 15.03354914759215966, -12.96403794047452607, -1.500000000000002220 ) ) ;
#28178=VECTOR ( 'NONE', #89117, 1000.000000000000114 ) ;
#28179=CARTESIAN_POINT ( 'NONE',  ( -109.5895376238167387, -24.64898659630368627, 1.056161002820390049 ) ) ;
#28180=CARTESIAN_POINT ( 'NONE',  ( 14.33573519231038063, 13.56928687979844561, -1.500000000000002220 ) ) ;
#28181=CARTESIAN_POINT ( 'NONE',  ( -42.58143151915821534, -24.51314013834315375, 0.6176544820404090697 ) ) ;
#28183=CARTESIAN_POINT ( 'NONE',  ( -110.5228709571500616, -24.51254535375845123, 9.355368624242252906 ) ) ;
#28185=CARTESIAN_POINT ( 'NONE',  ( -15.52656095410427817, -13.64048245868121434, 11.49999999999999645 ) ) ;
#28189=CARTESIAN_POINT ( 'NONE',  ( -12.60694655700363143, 18.86142483545513926, 11.49999999999999645 ) ) ;
#28194=CARTESIAN_POINT ( 'NONE',  ( -60.58953762381671737, -23.47593901973091235, -1.443836447539007972 ) ) ;
#28195=CARTESIAN_POINT ( 'NONE',  ( -36.62287095715005592, -23.48783264082477729, -1.443836473390072372 ) ) ;
#28199=CARTESIAN_POINT ( 'NONE',  ( 17.53461989915211916, -14.66684187699354425, 11.49999999999998934 ) ) ;
#28200=CARTESIAN_POINT ( 'NONE',  ( -29.60196703136402263, -23.88187520205043057, -0.6495508823503304274 ) ) ;
#28201=CARTESIAN_POINT ( 'NONE',  ( -20.03152041342270806, -8.007337437543776915, -1.500000000000002220 ) ) ;
#28202=CARTESIAN_POINT ( 'NONE',  ( -113.5892018432855650, -24.35071581493543746, 9.817618358456018157 ) ) ;
#28203=FACE_OUTER_BOUND ( 'NONE', #24338, .T. ) ;
#28204=CARTESIAN_POINT ( 'NONE',  ( 22.10748686624256720, -4.471405416651531795, 11.49999999999999645 ) ) ;
#28206=PLANE ( 'NONE',  #62695 ) ;
#28207=CARTESIAN_POINT ( 'NONE',  ( 19.92286461850947887, -9.344431347164146473, 11.49999999999998934 ) ) ;
#28208=CARTESIAN_POINT ( 'NONE',  ( -44.60757519715500052, -23.73791477778911130, 11.05961554403170943 ) ) ;
#28209=CARTESIAN_POINT ( 'NONE',  ( -28.94649234366282187, -25.21724812713350872, 6.769412627959744633 ) ) ;
#28211=DIRECTION ( 'NONE',  ( -3.773278334453079618E-23, 0.9999999999976377785, 2.173523156925979975E-06 ) ) ;
#28212=DIRECTION ( 'NONE',  ( 0.000000000000000000, -0.9999999999976377785, -2.173523156925979128E-06 ) ) ;
#28213=VERTEX_POINT ( 'NONE', #19393 ) ;
#28214=CARTESIAN_POINT ( 'NONE',  ( -108.5228709571500758, -23.47593901973090524, -1.443836447538996204 ) ) ;
#28218=CARTESIAN_POINT ( 'NONE',  ( -104.5228709571500758, -24.65952944569305316, 1.056160979905702346 ) ) ;
#28220=CARTESIAN_POINT ( 'NONE',  ( 8.094744887094867281, -18.73235182305680624, -1.500000000000002220 ) ) ;
#28222=ORIENTED_EDGE ( 'NONE', *, *, #2856, .T. ) ;
#28224=CARTESIAN_POINT ( 'NONE',  ( -30.56674980027052513, -25.57033040079278052, 6.142048374048878046 ) ) ;
#28225=ADVANCED_FACE ( 'NONE', ( #73689, #67097, #34636 ), #11019, .T. ) ;
#28227=CARTESIAN_POINT ( 'NONE',  ( -71.60924725748338915, -25.03149666953593666, 6.721928064598928110 ) ) ;
#28228=EDGE_LOOP ( 'NONE', ( #59698, #41711, #86905, #74896 ) ) ;
#28229=CARTESIAN_POINT ( 'NONE',  ( -99.92287095715006728, -23.47596703998600631, 11.44779298504227860 ) ) ;
#28230=DIRECTION ( 'NONE',  ( -0.000000000000000000, 2.173523156925979552E-06, -0.9999999999976378895 ) ) ;
#28232=ORIENTED_EDGE ( 'NONE', *, *, #25163, .T. ) ;
#28233=CARTESIAN_POINT ( 'NONE',  ( -3.686900873480770002, -20.48319827837541141, -1.500000000000002220 ) ) ;
#28234=ORIENTED_EDGE ( 'NONE', *, *, #99387, .T. ) ;
#28235=FACE_OUTER_BOUND ( 'NONE', #54186, .T. ) ;
#28236=ORIENTED_EDGE ( 'NONE', *, *, #75095, .F. ) ;
#28237=CARTESIAN_POINT ( 'NONE',  ( -28.62287095715004881, -24.49675894734168580, 8.947790415257339092 ) ) ;
#28238=CARTESIAN_POINT ( 'NONE',  ( -115.5228709571500616, -24.14321612903115977, -0.2833117244521543565 ) ) ;
#28239=ORIENTED_EDGE ( 'NONE', *, *, #81187, .F. ) ;
#28240=ORIENTED_EDGE ( 'NONE', *, *, #18792, .F. ) ;
#28242=EDGE_CURVE ( 'NONE', #51651, #44226, #68573, .T. ) ;
#28245=CARTESIAN_POINT ( 'NONE',  ( -74.62287095715004170, -23.72747288104469376, -1.053458166803227014 ) ) ;
#28246=CARTESIAN_POINT ( 'NONE',  ( -19.88706384024380824, 9.709922325909349894, 11.49999999999999645 ) ) ;
#28247=ORIENTED_EDGE ( 'NONE', *, *, #24002, .T. ) ;
#28248=CARTESIAN_POINT ( 'NONE',  ( -108.5492820750298790, -24.65952944569305316, 1.056160979905706121 ) ) ;
#28250=CARTESIAN_POINT ( 'NONE',  ( 3.115699594417459473, -22.39947108414558485, -1.500000000000002220 ) ) ;
#28251=ADVANCED_FACE ( 'NONE', ( #46739 ), #555, .T. ) ;
#28252=B_SPLINE_CURVE_WITH_KNOTS ( 'NONE', 3,
 ( #29171, #68243, #100151, #21052, #67756, #23031 ),
 .UNSPECIFIED., .F., .F.,
 ( 4, 2, 4 ),
 ( 6.384118694777179670E-06, 0.001386860460836454026, 0.002767336802978130617 ),
 .UNSPECIFIED. ) ;
#28253=CARTESIAN_POINT ( 'NONE',  ( -99.42106458011447501, -25.30551355002305769, 5.055668188524513162 ) ) ;
#28255=EDGE_CURVE ( 'NONE', #37811, #15171, #36644, .T. ) ;
#28258=DIRECTION ( 'NONE',  ( -3.773278334453079618E-23, 0.9999999999976377785, 2.173523156925979975E-06 ) ) ;
#28259=B_SPLINE_SURFACE_WITH_KNOTS ( 'NONE', 3, 3, ( 
 ( #36336, #12982, #22083, #52559 ),
 ( #6380, #43947, #83493, #59684 ),
 ( #21095, #74879, #99213, #61680 ),
 ( #93097, #78368, #15971, #85995 ),
 ( #40326, #70277, #7868, #99698 ),
 ( #92597, #63174, #8871, #7363 ),
 ( #94100, #16469, #93594, #257 ) ),
 .UNSPECIFIED., .F., .F., .F.,
 ( 4, 3, 4 ),
 ( 4, 4 ),
 ( 0.0004766839783816336743, 0.1029713700210892480, 0.2054660560637968647 ),
 ( 0.9397330492811201141, 0.9411793649393953576 ),
 .UNSPECIFIED. ) ;
#28261=ORIENTED_EDGE ( 'NONE', *, *, #13018, .T. ) ;
#28263=CARTESIAN_POINT ( 'NONE',  ( 20.12748746789148413, 9.599020362109589755, -1.500000000000002220 ) ) ;
#28264=CARTESIAN_POINT ( 'NONE',  ( -46.62287095715004170, -24.50216790748097395, 0.6166512839513648148 ) ) ;
#28265=EDGE_CURVE ( 'NONE', #52247, #86024, #5195, .T. ) ;
#28267=DIRECTION ( 'NONE',  ( -3.773278334453080206E-23, 0.9999999999976377785, 2.173523156925979975E-06 ) ) ;
#28268=DIRECTION ( 'NONE',  ( 0.000000000000000000, -2.173523156925979552E-06, 0.9999999999976378895 ) ) ;
#28271=CARTESIAN_POINT ( 'NONE',  ( -15.27948257512286645, 12.15582775940324822, -1.500000000000002220 ) ) ;
#28272=CARTESIAN_POINT ( 'NONE',  ( 20.52986552169224410, -6.224258026782483633, 11.49999999999998934 ) ) ;
#28275=DIRECTION ( 'NONE',  ( 3.773278334444166432E-23, -1.000000000000000000, 0.000000000000000000 ) ) ;
#28276=CARTESIAN_POINT ( 'NONE',  ( -21.78311099772515647, -6.823855485095160489, -1.500000000000002220 ) ) ;
#28279=DIRECTION ( 'NONE',  ( -3.773278334453079030E-23, 0.9999999999976377785, 2.173523156925979128E-06 ) ) ;
#28280=PLANE ( 'NONE',  #15213 ) ;
#28281=CARTESIAN_POINT ( 'NONE',  ( 8.874027960929927517, 17.90919871486395465, 11.49999999999999645 ) ) ;
#28282=CARTESIAN_POINT ( 'NONE',  ( -50.52287095715006160, -23.48783264082477018, -1.443836473390095021 ) ) ;
#28283=CARTESIAN_POINT ( 'NONE',  ( -57.62287095715004881, -23.48786465467241058, 11.44779295918254824 ) ) ;
#28284=CARTESIAN_POINT ( 'NONE',  ( -48.57734287085806102, -24.65952944569304606, 1.056160979905697239 ) ) ;
#28285=ORIENTED_EDGE ( 'NONE', *, *, #92769, .F. ) ;
#28286=DIRECTION ( 'NONE',  ( 0.000000000000000000, 0.9999999999976377785, 2.173523156925979128E-06 ) ) ;
#28287=EDGE_CURVE ( 'NONE', #51004, #51553, #24887, .T. ) ;
#28290=CARTESIAN_POINT ( 'NONE',  ( 9.217229664113554932, 19.63635308506117383, 11.49999999999998934 ) ) ;
#28291=CARTESIAN_POINT ( 'NONE',  ( -92.62287095715005592, -23.48783264082479150, -1.443836473390063713 ) ) ;
#28292=CARTESIAN_POINT ( 'NONE',  ( 3.395600993332231532, 19.23619202488179525, -1.500000000000002220 ) ) ;
#28294=EDGE_CURVE ( 'NONE', #38212, #71187, #29451, .T. ) ;
#28298=CARTESIAN_POINT ( 'NONE',  ( -52.62287095715006302, -24.65952944569304250, 1.056160979905695685 ) ) ;
#28299=CARTESIAN_POINT ( 'NONE',  ( 20.14718400222343320, -3.498931157112906476, 11.49999999999999645 ) ) ;
#28301=B_SPLINE_CURVE_WITH_KNOTS ( 'NONE', 3,
 ( #74161, #12241, #96996, #56456, #10260, #87888 ),
 .UNSPECIFIED., .F., .F.,
 ( 4, 2, 4 ),
 ( 6.391158118967745954E-06, 0.001387004593080787013, 0.002767618028042606333 ),
 .UNSPECIFIED. ) ;
#28302=DIRECTION ( 'NONE',  ( -3.773278334453079618E-23, 0.9999999999976377785, 2.173523156925979975E-06 ) ) ;
#28303=ORIENTED_EDGE ( 'NONE', *, *, #4320, .T. ) ;
#28304=EDGE_CURVE ( 'NONE', #43699, #70639, #25897, .T. ) ;
#28306=CARTESIAN_POINT ( 'NONE',  ( -43.62287095715004881, -24.66019654487199020, 8.947790411086135265 ) ) ;
#28307=CARTESIAN_POINT ( 'NONE',  ( -116.5581118885402958, -23.48786465467241769, 11.44779295918253759 ) ) ;
#28309=DIRECTION ( 'NONE',  ( -0.000000000000000000, 2.173523156925979552E-06, -0.9999999999976378895 ) ) ;
#28310=ORIENTED_EDGE ( 'NONE', *, *, #57484, .T. ) ;
#28312=CARTESIAN_POINT ( 'NONE',  ( -22.55714481399219906, -4.634528848986672500, 11.49999999999999645 ) ) ;
#28313=CARTESIAN_POINT ( 'NONE',  ( -7.601706241105644857, -21.46296766604531570, 11.49999999999998934 ) ) ;
#28315=PLANE ( 'NONE',  #70635 ) ;
#28316=CARTESIAN_POINT ( 'NONE',  ( -31.62287095715005236, -29.50250243563736774, 8.947779886222150481 ) ) ;
#28317=VECTOR ( 'NONE', #20397, 1000.000000000000114 ) ;
#28318=B_SPLINE_CURVE_WITH_KNOTS ( 'NONE', 3,
 ( #46937, #39314, #70274, #755, #75878, #53568 ),
 .UNSPECIFIED., .F., .F.,
 ( 4, 2, 4 ),
 ( 1.570755371634376281E-05, 0.001396183895866089271, 0.002776660238015834711 ),
 .UNSPECIFIED. ) ;
#28319=CARTESIAN_POINT ( 'NONE',  ( -90.62287095715004170, -24.99132157543084531, 2.256160258750667502 ) ) ;
#28320=CARTESIAN_POINT ( 'NONE',  ( -110.5864157058229296, -24.92564183028978775, 1.928384488918251982 ) ) ;
#28321=CARTESIAN_POINT ( 'NONE',  ( 17.35060923807083810, -13.37414737355047656, -1.500000000000002220 ) ) ;
#28325=CARTESIAN_POINT ( 'NONE',  ( -71.45309080802084623, -25.30256279997297497, 5.292638313163490871 ) ) ;
#28326=DIRECTION ( 'NONE',  ( -3.773278334453079030E-23, 0.9999999999976377785, 2.173523156925978705E-06 ) ) ;
#28327=EDGE_LOOP ( 'NONE', ( #44326, #70534, #7393, #24440 ) ) ;
#28328=CARTESIAN_POINT ( 'NONE',  ( 10.78675619948152864, -17.38023510967517637, -1.500000000000002220 ) ) ;
#28329=ORIENTED_EDGE ( 'NONE', *, *, #64015, .T. ) ;
#28330=ORIENTED_EDGE ( 'NONE', *, *, #23504, .F. ) ;
#28331=ORIENTED_EDGE ( 'NONE', *, *, #90780, .F. ) ;
#28332=CARTESIAN_POINT ( 'NONE',  ( 13.09964176094197441, 18.96253433080681106, 11.49999999999998934 ) ) ;
#28333=CARTESIAN_POINT ( 'NONE',  ( -61.49060039123366295, -24.65952944569304606, 1.056160979905699682 ) ) ;
#28334=CARTESIAN_POINT ( 'NONE',  ( -20.01257119864951051, 2.908879540851186274, -1.500000000000002220 ) ) ;
#28336=CARTESIAN_POINT ( 'NONE',  ( -98.62287095715009855, -24.33927499327854704, 9.819080762295815390 ) ) ;
#28340=CARTESIAN_POINT ( 'NONE',  ( 9.091334071971768793, -19.38302982324925239, 11.49999999999999645 ) ) ;
#28342=DIRECTION ( 'NONE',  ( -0.000000000000000000, 2.173523156925979552E-06, -0.9999999999976378895 ) ) ;
#28343=VERTEX_POINT ( 'NONE', #17282 ) ;
#28344=CARTESIAN_POINT ( 'NONE',  ( -7.755428854246955161, -20.87388092083558888, -1.500000000000002220 ) ) ;
#28345=CARTESIAN_POINT ( 'NONE',  ( 18.79598114143782084, -8.675585332008726169, -1.500000000000002220 ) ) ;
#28346=VECTOR ( 'NONE', #5099, 1000.000000000000227 ) ;
#28347=ORIENTED_EDGE ( 'NONE', *, *, #8107, .F. ) ;
#28349=VERTEX_POINT ( 'NONE', #79175 ) ;
#28352=CARTESIAN_POINT ( 'NONE',  ( -20.67734376658059858, -3.193854526364364954, -1.500000000000002220 ) ) ;
#28354=CARTESIAN_POINT ( 'NONE',  ( 12.66425630052701479, 17.85959152241435177, 11.49999999999999645 ) ) ;
#28356=CARTESIAN_POINT ( 'NONE',  ( -69.34303308397305443, -29.50249648326654039, 6.209198155459374924 ) ) ;
#28357=CARTESIAN_POINT ( 'NONE',  ( -11.40494320173684351, 19.43794304404440254, -1.500000000000002220 ) ) ;
#28359=CARTESIAN_POINT ( 'NONE',  ( 20.89173079421859214, 1.537965369061287557, 11.49999999999998934 ) ) ;
#28361=CARTESIAN_POINT ( 'NONE',  ( -91.52287095715003318, -23.48783264082477018, -1.443836473390089248 ) ) ;
#28363=ORIENTED_EDGE ( 'NONE', *, *, #6760, .F. ) ;
#28365=ORIENTED_EDGE ( 'NONE', *, *, #42967, .T. ) ;
#28366=ORIENTED_EDGE ( 'NONE', *, *, #21976, .F. ) ;
#28369=CARTESIAN_POINT ( 'NONE',  ( 21.15477495681221143, 3.540436534888726783, -1.500000000000002220 ) ) ;
#28370=CARTESIAN_POINT ( 'NONE',  ( -86.62287095715005592, -23.48786465467241413, 11.44779295918254469 ) ) ;
#28372=CARTESIAN_POINT ( 'NONE',  ( 7.532573551308565207, 19.69859070278346991, -1.500000000000002220 ) ) ;
#28373=CARTESIAN_POINT ( 'NONE',  ( -92.52287095715006160, -24.64965694238407323, 8.947790433994196491 ) ) ;
#28374=CARTESIAN_POINT ( 'NONE',  ( -124.6228709571500559, -24.64965695001469115, 8.947790433994175174 ) ) ;
#28375=CARTESIAN_POINT ( 'NONE',  ( -57.52287095715005449, -24.65952944569304606, 1.056160979905695463 ) ) ;
#28378=CARTESIAN_POINT ( 'NONE',  ( -19.88706384024380824, 9.709922325909349894, -1.500000000000002220 ) ) ;
#28381=DIRECTION ( 'NONE',  ( -3.773278334453080206E-23, 0.9999999999976377785, 2.173523156925979975E-06 ) ) ;
#28382=CARTESIAN_POINT ( 'NONE',  ( -99.52287095715010423, -23.95044443724993144, 10.65354141964649592 ) ) ;
#28383=CARTESIAN_POINT ( 'NONE',  ( -100.5221652074179701, -23.48783264082477018, -1.443836473390090580 ) ) ;
#28384=CARTESIAN_POINT ( 'NONE',  ( -19.30698013599780083, -2.078282243779251637, 11.49999999999998934 ) ) ;
#28386=CARTESIAN_POINT ( 'NONE',  ( 15.73328655151706101, -14.44092690703295467, 11.49999999999998934 ) ) ;
#28387=PLANE ( 'NONE',  #46681 ) ;
#28388=CARTESIAN_POINT ( 'NONE',  ( -48.85723664563188606, -25.20650842489795451, 6.812665538484691474 ) ) ;
#28389=CARTESIAN_POINT ( 'NONE',  ( -56.62287095715005592, -29.50248528299804818, 1.056150453629034924 ) ) ;
#28390=DIRECTION ( 'NONE',  ( -1.000000000000000000, -3.773278334444167608E-23, -8.201307833595939069E-29 ) ) ;
#28391=CARTESIAN_POINT ( 'NONE',  ( -21.91535228782390732, -5.629186751109307885, -1.500000000000002220 ) ) ;
#28394=CARTESIAN_POINT ( 'NONE',  ( -62.62287095715004881, -24.66019654487199020, 8.947790411086131712 ) ) ;
#28395=CARTESIAN_POINT ( 'NONE',  ( -4.105667982141768313, -19.37954422259287668, 11.49999999999999645 ) ) ;
#28399=LINE ( 'NONE', #37021, #96047 ) ;
#28400=FACE_OUTER_BOUND ( 'NONE', #63018, .T. ) ;
#28401=CARTESIAN_POINT ( 'NONE',  ( -100.7619115510279926, -25.17353336829146926, 7.069363366734568110 ) ) ;
#28402=CARTESIAN_POINT ( 'NONE',  ( -18.67883320684159543, -10.89015303950203517, -1.500000000000002220 ) ) ;
#28403=DIRECTION ( 'NONE',  ( -3.773278334453079030E-23, 0.9999999999976377785, 2.173523156925979128E-06 ) ) ;
#28404=CARTESIAN_POINT ( 'NONE',  ( -8.550378450311910683, 17.38971893761031851, -1.500000000000002220 ) ) ;
#28406=CARTESIAN_POINT ( 'NONE',  ( -94.62287095715005592, -29.50248528299804818, 1.056150453629040253 ) ) ;
#28407=CARTESIAN_POINT ( 'NONE',  ( -11.05534852661189937, -16.44151763790470966, -1.500000000000002220 ) ) ;
#28408=EDGE_CURVE ( 'NONE', #26747, #86903, #79063, .T. ) ;
#28409=ORIENTED_EDGE ( 'NONE', *, *, #41434, .F. ) ;
#28410=CARTESIAN_POINT ( 'NONE',  ( -12.21837793623082113, -16.16665877782589433, 11.49999999999999645 ) ) ;
#28411=CARTESIAN_POINT ( 'NONE',  ( -119.5228709571500758, -23.96177878511309345, 10.65340807706329151 ) ) ;
#28413=EDGE_CURVE ( 'NONE', #71294, #38181, #37913, .T. ) ;
#28414=DIRECTION ( 'NONE',  ( -3.773278334453079030E-23, 0.9999999999976377785, 2.173523156925979128E-06 ) ) ;
#28415=ORIENTED_EDGE ( 'NONE', *, *, #60045, .T. ) ;
#28416=FACE_OUTER_BOUND ( 'NONE', #43334, .T. ) ;
#28417=CARTESIAN_POINT ( 'NONE',  ( -50.52287095715006160, -29.50250786944525672, 11.44777988621624054 ) ) ;
#28418=CARTESIAN_POINT ( 'NONE',  ( -51.04357394935764347, -29.50249372652338664, 4.940868828539293212 ) ) ;
#28421=CARTESIAN_POINT ( 'NONE',  ( -1.723993941171178879, -19.98520929721398431, -1.500000000000002220 ) ) ;
#28422=B_SPLINE_CURVE_WITH_KNOTS ( 'NONE', 3,
 ( #73273, #27092, #11366, #3767 ),
 .UNSPECIFIED., .F., .F.,
 ( 4, 4 ),
 ( 1.387778780781445521E-17, 0.001341346153846192935 ),
 .UNSPECIFIED. ) ;
#28426=AXIS2_PLACEMENT_3D ( 'NONE', #8862, #47934, #15963 ) ;
#28427=CARTESIAN_POINT ( 'NONE',  ( -49.68676680831369197, -25.31297152054679245, 4.434853371053554483 ) ) ;
#28431=EDGE_CURVE ( 'NONE', #65949, #90027, #23330, .T. ) ;
#28432=DIRECTION ( 'NONE',  ( 0.000000000000000000, 2.173523156925980399E-06, -0.9999999999976378895 ) ) ;
#28433=CARTESIAN_POINT ( 'NONE',  ( -10.09097066620046235, 20.03973272787133553, 11.49999999999999645 ) ) ;
#28436=CARTESIAN_POINT ( 'NONE',  ( 10.94010344783756672, -17.16519937159427656, 11.49999999999998934 ) ) ;
#28437=ORIENTED_EDGE ( 'NONE', *, *, #92617, .F. ) ;
#28438=CARTESIAN_POINT ( 'NONE',  ( 21.44032754495887261, 8.191337786432022483, 11.49999999999998934 ) ) ;
#28439=CARTESIAN_POINT ( 'NONE',  ( -61.52287095715006160, -24.64965694238407323, 8.947790433994201820 ) ) ;
#28443=EDGE_CURVE ( 'NONE', #27352, #94885, #39163, .T. ) ;
#28444=CARTESIAN_POINT ( 'NONE',  ( -67.52287095715007581, -24.50321055353805733, 9.387540953477515160 ) ) ;
#28446=CARTESIAN_POINT ( 'NONE',  ( -21.15187133135857422, -0.9709546189074961253, 11.49999999999999645 ) ) ;
#28450=CARTESIAN_POINT ( 'NONE',  ( -20.56814720681451902, 8.302189128749821734, -1.500000000000002220 ) ) ;
#28451=CARTESIAN_POINT ( 'NONE',  ( 7.647619880454145758, 19.11525441646967849, 11.49999999999998934 ) ) ;
#28452=ORIENTED_EDGE ( 'NONE', *, *, #173, .T. ) ;
#28455=B_SPLINE_CURVE_WITH_KNOTS ( 'NONE', 3,
 ( #33657, #94544, #57009, #25032 ),
 .UNSPECIFIED., .F., .F.,
 ( 4, 4 ),
 ( 0.8393800999571321420, 0.8403808469978977236 ),
 .UNSPECIFIED. ) ;
#28456=CARTESIAN_POINT ( 'NONE',  ( -126.6228709571500559, -24.35013146730204525, 9.818937971375094165 ) ) ;
#28457=ORIENTED_EDGE ( 'NONE', *, *, #99124, .F. ) ;
#28458=ORIENTED_EDGE ( 'NONE', *, *, #19534, .T. ) ;
#28459=B_SPLINE_CURVE_WITH_KNOTS ( 'NONE', 3,
 ( #99010, #73819, #4322, #19526, #67596, #45743, #50004, #21384, #30006, #30510, #90916, #61479, #53366, #52361, #44751, #83295, #11424, #13775 ),
 .UNSPECIFIED., .F., .F.,
 ( 4, 2, 2, 2, 2, 2, 2, 2, 4 ),
 ( 0.000000000000000000, 0.0002960763747946566164, 0.0005921527495893132327, 0.0008882291243839698491, 0.001184305499178626465, 0.001480381873973283082, 0.001776458248767939698, 0.002072534623562596531, 0.002368610998357252931 ),
 .UNSPECIFIED. ) ;
#28462=DIRECTION ( 'NONE',  ( 1.000000000000000000, 3.773278334444167608E-23, 8.201307833595939069E-29 ) ) ;
#28463=CARTESIAN_POINT ( 'NONE',  ( -28.61148789775794654, -23.58142141106679546, 11.05961558438220749 ) ) ;
#28464=CARTESIAN_POINT ( 'NONE',  ( -49.10457154551149728, -25.27419814425984512, 3.999772249604824914 ) ) ;
#28465=CARTESIAN_POINT ( 'NONE',  ( -20.46667790307254009, -3.548193229090686796, -1.500000000000002220 ) ) ;
#28466=EDGE_CURVE ( 'NONE', #55720, #61817, #7530, .T. ) ;
#28467=CARTESIAN_POINT ( 'NONE',  ( 21.72137571921558319, 1.130696696492564213, 11.49999999999999645 ) ) ;
#28468=ORIENTED_EDGE ( 'NONE', *, *, #36713, .F. ) ;
#28469=CARTESIAN_POINT ( 'NONE',  ( -40.91098280806539833, -25.31583749408676809, 4.981853969359134382 ) ) ;
#28471=CARTESIAN_POINT ( 'NONE',  ( -115.6239652621308664, -24.92564183028979130, 1.928384488918252870 ) ) ;
#28472=CARTESIAN_POINT ( 'NONE',  ( 4.981011153104904388, 21.88276397462241363, -1.500000000000002220 ) ) ;
#28473=CARTESIAN_POINT ( 'NONE',  ( -51.29687923781917647, -25.26334590255974533, 3.993462177038400895 ) ) ;
#28474=CARTESIAN_POINT ( 'NONE',  ( -102.5228709571500758, -24.64965694238407323, 8.947790433994194714 ) ) ;
#28476=CARTESIAN_POINT ( 'NONE',  ( -71.67926322476502321, -25.28257675302215901, 5.899957443109282273 ) ) ;
#28477=CARTESIAN_POINT ( 'NONE',  ( -77.62287095715009855, -23.47596703998600631, 11.44779298504227683 ) ) ;
#28478=ORIENTED_EDGE ( 'NONE', *, *, #76044, .T. ) ;
#28479=ORIENTED_EDGE ( 'NONE', *, *, #36961, .F. ) ;
#28484=CARTESIAN_POINT ( 'NONE',  ( -4.730540317195566224, 20.75322969461001676, -1.500000000000002220 ) ) ;
#28485=ADVANCED_FACE ( 'NONE', ( #50741 ), #60236, .F. ) ;
#28487=CARTESIAN_POINT ( 'NONE',  ( -80.52287095715004739, -25.00182538069145366, 7.747789668545104647 ) ) ;
#28489=CARTESIAN_POINT ( 'NONE',  ( 9.643594380127815668, 19.59848315111488759, -1.500000000000002220 ) ) ;
#28491=CARTESIAN_POINT ( 'NONE',  ( 12.08046422559826816, 19.21373320108137861, -1.500000000000002220 ) ) ;
#28492=CARTESIAN_POINT ( 'NONE',  ( -40.75388878839229534, -25.28892429803972774, 3.329423022938666765 ) ) ;
#28495=CARTESIAN_POINT ( 'NONE',  ( -0.1377007522546883911, -21.91379463844567965, -1.500000000000002220 ) ) ;
#28496=CARTESIAN_POINT ( 'NONE',  ( -39.52287095715004739, -24.34917612406835730, 0.1852690917426483286 ) ) ;
#28498=CARTESIAN_POINT ( 'NONE',  ( -122.6239430697742847, -24.51419770103158413, 9.386484678747169852 ) ) ;
#28500=AXIS2_PLACEMENT_3D ( 'NONE', #82672, #97403, #76541 ) ;
#28503=ORIENTED_EDGE ( 'NONE', *, *, #1033, .F. ) ;
#28504=FACE_OUTER_BOUND ( 'NONE', #3967, .T. ) ;
#28507=CARTESIAN_POINT ( 'NONE',  ( -15.80959461918071618, 14.24510877297761446, -1.500000000000002220 ) ) ;
#28508=CARTESIAN_POINT ( 'NONE',  ( -98.62739836056972820, -24.35071581493543746, 9.817618358456027039 ) ) ;
#28509=CARTESIAN_POINT ( 'NONE',  ( -26.12582186233688830, -24.97064840753675341, 4.293463527599305607 ) ) ;
#28510=CARTESIAN_POINT ( 'NONE',  ( -114.5228709571500474, -24.51283580621455371, 0.6167428607046516742 ) ) ;
#28511=CARTESIAN_POINT ( 'NONE',  ( -29.58953762381673869, -23.40614417124189117, -1.443836160644816680 ) ) ;
#28512=CARTESIAN_POINT ( 'NONE',  ( -117.5912915777627177, -23.96169478059714564, 10.65365249895717170 ) ) ;
#28514=CARTESIAN_POINT ( 'NONE',  ( -10.41718274906430786, -16.55731393670301088, 11.49999999999999645 ) ) ;
#28515=CARTESIAN_POINT ( 'NONE',  ( -66.62287095715009855, -23.73934037231756733, 11.05740245334329153 ) ) ;
#28518=PLANE ( 'NONE',  #94377 ) ;
#28519=CARTESIAN_POINT ( 'NONE',  ( -101.9326655587415331, -25.23357337914073995, 6.326899518756052387 ) ) ;
#28520=B_SPLINE_CURVE_WITH_KNOTS ( 'NONE', 3,
 ( #45464, #61688, #60192, #98729 ),
 .UNSPECIFIED., .F., .F.,
 ( 4, 4 ),
 ( 0.000000000000000000, 9.999999999999592548E-05 ),
 .UNSPECIFIED. ) ;
#28521=CARTESIAN_POINT ( 'NONE',  ( -116.5895376238167387, -23.48783264082478794, -1.443836473390058606 ) ) ;
#28522=CARTESIAN_POINT ( 'NONE',  ( -106.5228709571500758, -24.65952944569305316, 1.056160979905704123 ) ) ;
#28524=CARTESIAN_POINT ( 'NONE',  ( -16.18664964019209052, -11.25563402961023662, -1.500000000000002220 ) ) ;
#28525=VERTEX_POINT ( 'NONE', #81182 ) ;
#28529=ORIENTED_EDGE ( 'NONE', *, *, #1623, .F. ) ;
#28532=CARTESIAN_POINT ( 'NONE',  ( -47.63994789387633944, -24.15543982623907127, -0.2315651400026536022 ) ) ;
#28533=CARTESIAN_POINT ( 'NONE',  ( -118.5879173097015240, -24.65952944569305316, 1.056160979905708119 ) ) ;
#28535=DIRECTION ( 'NONE',  ( 0.000000000000000000, -2.173523156925980399E-06, 0.9999999999976378895 ) ) ;
#28536=CARTESIAN_POINT ( 'NONE',  ( -116.5228709571500616, -29.50250243563736774, 8.947779886222134493 ) ) ;
#28537=CARTESIAN_POINT ( 'NONE',  ( -7.409219584043468920, -18.53548363135739052, 11.49999999999998934 ) ) ;
#28539=CARTESIAN_POINT ( 'NONE',  ( -0.03226556487338757412, -22.63229690711892772, 1.846386587601361651 ) ) ;
#28540=EDGE_LOOP ( 'NONE', ( #25955, #11490, #10768, #53913 ) ) ;
#28541=CARTESIAN_POINT ( 'NONE',  ( -128.5228709571500758, -23.48786465467242479, 11.44779295918253581 ) ) ;
#28545=FACE_OUTER_BOUND ( 'NONE', #98402, .T. ) ;
#28546=DIRECTION ( 'NONE',  ( 0.000000000000000000, -2.173523156925980399E-06, 0.9999999999976378895 ) ) ;
#28547=CARTESIAN_POINT ( 'NONE',  ( -125.0507906094695585, -25.24724330731294231, 6.200220586889952479 ) ) ;
#28548=CARTESIAN_POINT ( 'NONE',  ( -81.62949391327481408, -24.34968618360933945, 0.1864209137778954084 ) ) ;
#28553=EDGE_CURVE ( 'NONE', #61715, #57842, #17235, .T. ) ;
#28555=CARTESIAN_POINT ( 'NONE',  ( -79.62287095715007013, -24.35013146730204525, 9.818937971375108376 ) ) ;
#28558=VERTEX_POINT ( 'NONE', #53118 ) ;
#28559=VECTOR ( 'NONE', #63717, 1000.000000000000114 ) ;
#28560=CARTESIAN_POINT ( 'NONE',  ( 19.26017855675105750, 6.235128648364509196, 11.49999999999998934 ) ) ;
#28561=B_SPLINE_CURVE_WITH_KNOTS ( 'NONE', 3,
 ( #41568, #18702, #81114, #64425 ),
 .UNSPECIFIED., .F., .F.,
 ( 4, 4 ),
 ( 0.000000000000000000, 9.999999999998897304E-05 ),
 .UNSPECIFIED. ) ;
#28562=CARTESIAN_POINT ( 'NONE',  ( -69.67778434337223814, -25.31561343761894634, 4.981274948899643285 ) ) ;
#28565=EDGE_CURVE ( 'NONE', #55078, #70110, #12374, .T. ) ;
#28566=EDGE_CURVE ( 'NONE', #96746, #83609, #94693, .T. ) ;
#28567=AXIS2_PLACEMENT_3D ( 'NONE', #68753, #38791, #69246 ) ;
#28571=CARTESIAN_POINT ( 'NONE',  ( -79.97841713288102028, -25.30708236192187854, 4.547326657696674879 ) ) ;
#28572=CARTESIAN_POINT ( 'NONE',  ( -52.52287095715005449, -24.35013146730203104, 9.818937971375113705 ) ) ;
#28573=CARTESIAN_POINT ( 'NONE',  ( 1.781536345648733199, 20.00535218256611358, -1.500000000000002220 ) ) ;
#28574=CARTESIAN_POINT ( 'NONE',  ( -17.33045254171255678, -11.89390297951003816, 11.49999999999999645 ) ) ;
#28576=CARTESIAN_POINT ( 'NONE',  ( -29.11574841292185312, -25.12648593425884513, 6.386170400369471700 ) ) ;
#28577=CARTESIAN_POINT ( 'NONE',  ( -70.58914684821826313, -24.52399227489126687, 9.353111116836529959 ) ) ;
#28578=CARTESIAN_POINT ( 'NONE',  ( -22.03165466229905789, 1.424673820674137614, 11.49999999999998934 ) ) ;
#28579=CARTESIAN_POINT ( 'NONE',  ( -47.22287095715005023, -23.47596703998600276, 11.44779298504227683 ) ) ;
#28581=CARTESIAN_POINT ( 'NONE',  ( -34.52287095715006160, -29.50248528299804818, 1.056150453629029817 ) ) ;
#28583=CARTESIAN_POINT ( 'NONE',  ( -99.12732697106135049, -25.26762180873494756, 3.920099948859327554 ) ) ;
#28584=CARTESIAN_POINT ( 'NONE',  ( -31.57094520315825648, -23.48783264082477018, -1.443836473390079256 ) ) ;
#28586=ORIENTED_EDGE ( 'NONE', *, *, #20269, .T. ) ;
#28587=CARTESIAN_POINT ( 'NONE',  ( -49.52287095715006160, -23.47596703998600631, 11.44779298504229104 ) ) ;
#28588=CARTESIAN_POINT ( 'NONE',  ( -106.6228709571500559, -23.48786465467241769, 11.44779295918253759 ) ) ;
#28589=CARTESIAN_POINT ( 'NONE',  ( -48.52287095715006160, -24.66019654487200086, 8.947790411086119278 ) ) ;
#28590=B_SPLINE_CURVE_WITH_KNOTS ( 'NONE', 3,
 ( #4484, #3488, #57774, #2991 ),
 .UNSPECIFIED., .F., .F.,
 ( 4, 4 ),
 ( 0.7710505883516606263, 0.7800570196237761600 ),
 .UNSPECIFIED. ) ;
#28591=CARTESIAN_POINT ( 'NONE',  ( 20.58124611042576646, 0.8182449333618511123, -1.500000000000002220 ) ) ;
#28594=CARTESIAN_POINT ( 'NONE',  ( -17.63906703526961550, 12.34593017946836291, 11.49999999999999645 ) ) ;
#28595=ORIENTED_EDGE ( 'NONE', *, *, #26986, .T. ) ;
#28596=CARTESIAN_POINT ( 'NONE',  ( -48.62287095715004881, -24.64965695001467694, 8.947790433994185832 ) ) ;
#28597=CARTESIAN_POINT ( 'NONE',  ( -99.49719608488790357, -25.30438760448027935, 4.819451417661368531 ) ) ;
#28600=CARTESIAN_POINT ( 'NONE',  ( 21.44611857939883137, 6.294191480875499067, 11.49999999999998934 ) ) ;
#28601=CARTESIAN_POINT ( 'NONE',  ( -93.52287095715006160, -23.47593901973090524, -1.443836447538996648 ) ) ;
#28605=CARTESIAN_POINT ( 'NONE',  ( -110.5228709571500616, -25.00158670708909625, 2.256160236439166411 ) ) ;
#28606=CARTESIAN_POINT ( 'NONE',  ( -48.22287095715007155, -23.47596703998600276, 11.44779298504227683 ) ) ;
#28607=B_SPLINE_CURVE_WITH_KNOTS ( 'NONE', 3,
 ( #11475, #43930, #34822, #19582 ),
 .UNSPECIFIED., .F., .F.,
 ( 4, 4 ),
 ( 0.000000000000000000, 9.999999999997510880E-05 ),
 .UNSPECIFIED. ) ;
#28608=CARTESIAN_POINT ( 'NONE',  ( 20.33208665566141704, 4.825383418962623239, 11.49999999999998934 ) ) ;
#28612=ORIENTED_EDGE ( 'NONE', *, *, #71348, .T. ) ;
#28614=CARTESIAN_POINT ( 'NONE',  ( -100.5087600408661928, -24.63419186844611275, 9.035850630976915099 ) ) ;
#28615=CARTESIAN_POINT ( 'NONE',  ( 11.82777538550527119, 17.46297031709455183, -1.500000000000002220 ) ) ;
#28616=ORIENTED_EDGE ( 'NONE', *, *, #55762, .F. ) ;
#28617=CARTESIAN_POINT ( 'NONE',  ( -60.52287095715006160, -24.99156044556119838, 7.747789690856173195 ) ) ;
#28619=CARTESIAN_POINT ( 'NONE',  ( -120.5222358195599810, -23.48786465467241769, 11.44779295918253936 ) ) ;
#28620=CARTESIAN_POINT ( 'NONE',  ( -76.63827036425878703, -23.96169478059713143, 10.65365249895718058 ) ) ;
#28621=CARTESIAN_POINT ( 'NONE',  ( -74.62287095715005592, -24.65952944569304606, 1.056160979905696351 ) ) ;
#28622=CARTESIAN_POINT ( 'NONE',  ( -3.058130702743298901, -21.54894043062209263, -1.500000000000002220 ) ) ;
#28623=CARTESIAN_POINT ( 'NONE',  ( -98.62287095715005592, -23.48786465467241769, 11.44779295918254292 ) ) ;
#28624=CARTESIAN_POINT ( 'NONE',  ( -14.53400517605410158, 16.95891092046126403, 11.49999999999999645 ) ) ;
#28625=ORIENTED_EDGE ( 'NONE', *, *, #67772, .T. ) ;
#28626=CARTESIAN_POINT ( 'NONE',  ( -57.52287095715003318, -24.66019654487198665, 8.947790411086121054 ) ) ;
#28629=EDGE_CURVE ( 'NONE', #56116, #62739, #53554, .T. ) ;
#28630=ORIENTED_EDGE ( 'NONE', *, *, #15364, .F. ) ;
#28632=ADVANCED_FACE ( 'NONE', ( #91655 ), #92650, .F. ) ;
#28633=VERTEX_POINT ( 'NONE', #93147 ) ;
#28637=DIRECTION ( 'NONE',  ( -3.773278334453079618E-23, 0.9999999999976377785, 2.173523156925979975E-06 ) ) ;
#28640=CARTESIAN_POINT ( 'NONE',  ( -7.246369895950522277, -17.95243785538732340, -1.500000000000002220 ) ) ;
#28641=CARTESIAN_POINT ( 'NONE',  ( -51.27945410110257995, -25.31566608536513030, 5.069311121527179331 ) ) ;
#28644=CARTESIAN_POINT ( 'NONE',  ( 19.05472526407214673, 3.605321472892077050, 11.49999999999999645 ) ) ;
#28650=CARTESIAN_POINT ( 'NONE',  ( -64.52287095715006160, -29.50250243563736774, 8.947779886222145151 ) ) ;
#28652=CARTESIAN_POINT ( 'NONE',  ( -36.52287095715008292, -24.51387760970724017, 9.387446482453407626 ) ) ;
#28653=CARTESIAN_POINT ( 'NONE',  ( 19.03533760385612439, 4.641190475545474037, 11.49999999999998934 ) ) ;
#28656=CARTESIAN_POINT ( 'NONE',  ( -21.01953065494444317, -4.859126342152997324, -1.500000000000002220 ) ) ;
#28657=CARTESIAN_POINT ( 'NONE',  ( -86.52287095715006160, -23.47596703998600631, 11.44779298504228393 ) ) ;
#28660=CARTESIAN_POINT ( 'NONE',  ( -100.4008197971955667, -25.18439335906099075, 3.294680639966506508 ) ) ;
#28661=CARTESIAN_POINT ( 'NONE',  ( -22.94451526424785115, -1.264959178018935315, -1.500000000000002220 ) ) ;
#28664=CARTESIAN_POINT ( 'NONE',  ( -100.6814946224345846, -25.30401792888237367, 5.197789011716578145 ) ) ;
#28665=CARTESIAN_POINT ( 'NONE',  ( -4.233023369943174075, 19.68221892606961987, 11.49999999999999645 ) ) ;
#28666=CARTESIAN_POINT ( 'NONE',  ( -101.5562042904833930, -24.64898659630528499, 1.056161002820828143 ) ) ;
#28667=FACE_OUTER_BOUND ( 'NONE', #58174, .T. ) ;
#28668=B_SPLINE_CURVE_WITH_KNOTS ( 'NONE', 3,
 ( #12862, #30088, #38197, #83876, #100074, #14857 ),
 .UNSPECIFIED., .F., .F.,
 ( 4, 2, 4 ),
 ( 6.384118678611908238E-06, 0.001386860460828373900, 0.002767336802978135821 ),
 .UNSPECIFIED. ) ;
#28670=B_SPLINE_CURVE_WITH_KNOTS ( 'NONE', 3,
 ( #5985, #35939, #44555, #67400, #58293, #97341 ),
 .UNSPECIFIED., .F., .F.,
 ( 4, 2, 4 ),
 ( 0.000000000000000000, 0.001381510080715903652, 0.002763020161431807304 ),
 .UNSPECIFIED. ) ;
#28673=CARTESIAN_POINT ( 'NONE',  ( -17.31707178780640533, -9.736581320607820444, -1.500000000000002220 ) ) ;
#28674=PLANE ( 'NONE',  #4224 ) ;
#28675=CARTESIAN_POINT ( 'NONE',  ( 16.85830656838225039, -10.38424343889589707, -1.500000000000002220 ) ) ;
#28676=AXIS2_PLACEMENT_3D ( 'NONE', #41461, #59691, #27237 ) ;
#28680=CARTESIAN_POINT ( 'NONE',  ( 9.361532043782798240, 18.45020211870636118, 11.49999999999999645 ) ) ;
#28682=CARTESIAN_POINT ( 'NONE',  ( -99.16166289166535819, -25.30166215957521914, 5.311370747606397380 ) ) ;
#28684=CARTESIAN_POINT ( 'NONE',  ( -50.37830952628071657, -25.31439277241203101, 5.197788989166616247 ) ) ;
#28685=CARTESIAN_POINT ( 'NONE',  ( -17.38503614929206265, -14.63273120789127013, 11.49999999999999645 ) ) ;
#28687=B_SPLINE_SURFACE_WITH_KNOTS ( 'NONE', 3, 3, ( 
 ( #63853, #72447, #27270, #25762 ),
 ( #64860, #89165, #50603, #33367 ),
 ( #81556, #94767, #87666, #66844 ),
 ( #51104, #4928, #12528, #43497 ),
 ( #13520, #35875, #74435, #97274 ),
 ( #20141, #35386, #82047, #59723 ),
 ( #51602, #67837, #82540, #13020 ) ),
 .UNSPECIFIED., .F., .F., .F.,
 ( 4, 3, 4 ),
 ( 4, 4 ),
 ( 0.7945040050992244751, 0.8970133687736503436, 0.9995227324480762121 ),
 ( 0.7296794188957508309, 0.7310290118914040125 ),
 .UNSPECIFIED. ) ;
#28688=CARTESIAN_POINT ( 'NONE',  ( -46.62287095715004881, -24.66019654487198665, 8.947790411086135265 ) ) ;
#28694=CARTESIAN_POINT ( 'NONE',  ( -93.62287095715005592, -23.48786465467241769, 11.44779295918254114 ) ) ;
#28698=ADVANCED_FACE ( 'NONE', ( #38372 ), #24144, .F. ) ;
#28699=ORIENTED_EDGE ( 'NONE', *, *, #59191, .T. ) ;
#28700=LINE ( 'NONE', #5359, #85756 ) ;
#28701=B_SPLINE_CURVE_WITH_KNOTS ( 'NONE', 3,
 ( #28076, #59031, #60533, #35191, #74728, #5725, #52910, #45297, #67152, #98060, #28562, #91447, #13324, #43305, #75718, #90463 ),
 .UNSPECIFIED., .F., .F.,
 ( 4, 2, 2, 2, 2, 2, 2, 4 ),
 ( 0.000000000000000000, 0.0002615882740771409095, 0.0005231765481542818190, 0.001046353096308548242, 0.001307941370385681942, 0.001569529644462814991, 0.001831117918539948257, 0.002092706192617081306 ),
 .UNSPECIFIED. ) ;
#28702=CARTESIAN_POINT ( 'NONE',  ( 21.14566350062385780, -8.679158401671109857, -1.500000000000002220 ) ) ;
#28703=CARTESIAN_POINT ( 'NONE',  ( -29.54490261039654442, -24.07229224446866667, -0.2315648265717072385 ) ) ;
#28704=CARTESIAN_POINT ( 'NONE',  ( -2.376235263977734657, 21.45616117177731041, -1.500000000000002220 ) ) ;
#28705=CARTESIAN_POINT ( 'NONE',  ( -113.5517671225293128, -24.51419770103157347, 9.386484678747168076 ) ) ;
#28707=CARTESIAN_POINT ( 'NONE',  ( -10.21242994381667657, -20.12718729479640700, 11.49999999999999645 ) ) ;
#28708=VERTEX_POINT ( 'NONE', #23130 ) ;
#28709=DIRECTION ( 'NONE',  ( 0.000000000000000000, -2.173523156925980399E-06, 0.9999999999976378895 ) ) ;
#28710=CARTESIAN_POINT ( 'NONE',  ( -6.321128248299066499, 21.05883132939252533, -1.500000000000002220 ) ) ;
#28712=CARTESIAN_POINT ( 'NONE',  ( -105.5100248002994050, -24.73531770709095312, 8.716586749053508498 ) ) ;
#28713=CARTESIAN_POINT ( 'NONE',  ( -28.09930172958063466, -24.79700303329384425, 7.540558023410448563 ) ) ;
#28715=CARTESIAN_POINT ( 'NONE',  ( -89.62287095715008434, -23.73934037231757799, 11.05740245334328797 ) ) ;
#28716=CARTESIAN_POINT ( 'NONE',  ( -90.63102145325892423, -24.52399227489127398, 9.353111116836531735 ) ) ;
#28717=ORIENTED_EDGE ( 'NONE', *, *, #39910, .T. ) ;
#28719=VERTEX_POINT ( 'NONE', #68832 ) ;
#28721=ORIENTED_EDGE ( 'NONE', *, *, #1798, .T. ) ;
#28722=CARTESIAN_POINT ( 'NONE',  ( -49.28021062419514919, -25.26817783364414183, 6.077668871661954242 ) ) ;
#28724=CARTESIAN_POINT ( 'NONE',  ( -57.58284588185660624, -24.51314013834315375, 0.6176544820404114011 ) ) ;
#28725=CARTESIAN_POINT ( 'NONE',  ( 2.691128592823461840, 20.25793168094256202, -1.500000000000002220 ) ) ;
#28726=ADVANCED_FACE ( 'NONE', ( #92153 ), #85542, .T. ) ;
#28727=VERTEX_POINT ( 'NONE', #77418 ) ;
#28729=CARTESIAN_POINT ( 'NONE',  ( -30.59326697242301663, -24.88273649812090227, 8.549170486301877148 ) ) ;
#28730=CARTESIAN_POINT ( 'NONE',  ( -105.6382416112896436, -23.48783264082477018, -1.443836473390094355 ) ) ;
#28732=EDGE_CURVE ( 'NONE', #95160, #66603, #88593, .T. ) ;
#28735=CARTESIAN_POINT ( 'NONE',  ( -94.62287095715005592, -23.47593901973091235, -1.443836447539002865 ) ) ;
#28736=CARTESIAN_POINT ( 'NONE',  ( 2.677173591928626806, -20.63698567995287902, 11.49999999999998934 ) ) ;
#28737=ORIENTED_EDGE ( 'NONE', *, *, #73971, .F. ) ;
#28740=DIRECTION ( 'NONE',  ( 0.000000000000000000, 0.9999999999976377785, 2.173523156925979975E-06 ) ) ;
#28741=CARTESIAN_POINT ( 'NONE',  ( -129.5217890828018312, -24.66019654487200086, 8.947790411086113949 ) ) ;
#28746=CARTESIAN_POINT ( 'NONE',  ( -109.5228709571500616, -24.64898659630530275, 1.056161002820831474 ) ) ;
#28747=CARTESIAN_POINT ( 'NONE',  ( -71.29000553066028090, -25.24515197902177022, 6.029837115414142801 ) ) ;
#28748=CARTESIAN_POINT ( 'NONE',  ( -19.76278938440450617, -9.944092408650034187, 11.49999999999999645 ) ) ;
#28750=CARTESIAN_POINT ( 'NONE',  ( -75.52287095715006160, -29.50249982740957577, 7.747779886224967605 ) ) ;
#28751=CARTESIAN_POINT ( 'NONE',  ( 12.73759380600583846, -18.68238426224762350, -1.500000000000002220 ) ) ;
#28752=AXIS2_PLACEMENT_3D ( 'NONE', #20006, #42865, #43361 ) ;
#28753=EDGE_CURVE ( 'NONE', #92012, #27790, #43841, .T. ) ;
#28754=CARTESIAN_POINT ( 'NONE',  ( -115.5883522698519954, -24.73531770709096023, 8.716586749053508498 ) ) ;
#28755=VERTEX_POINT ( 'NONE', #77916 ) ;
#28756=ORIENTED_EDGE ( 'NONE', *, *, #8646, .T. ) ;
#28760=CARTESIAN_POINT ( 'NONE',  ( -7.807601069497579260, -18.53474111305376937, 11.49999999999998934 ) ) ;
#28763=CARTESIAN_POINT ( 'NONE',  ( -40.09822460666767086, -25.30507952954706852, 5.519450557857781270 ) ) ;
#28764=CARTESIAN_POINT ( 'NONE',  ( -17.00426676922356606, 14.40147940013276973, -1.500000000000002220 ) ) ;
#28765=CARTESIAN_POINT ( 'NONE',  ( -50.40895856474225667, -25.03220906767835885, 7.563174217889635287 ) ) ;
#28767=CARTESIAN_POINT ( 'NONE',  ( -110.5228709571500616, -23.48786465467242479, 11.44779295918253936 ) ) ;
#28768=FACE_OUTER_BOUND ( 'NONE', #4245, .T. ) ;
#28769=CARTESIAN_POINT ( 'NONE',  ( -109.8650282762807393, -29.50249556043354460, 5.784618828537300139 ) ) ;
#28771=DIRECTION ( 'NONE',  ( 0.5661055431922977776, 0.000000000000000000, -0.8243327689513219036 ) ) ;
#28773=CARTESIAN_POINT ( 'NONE',  ( -6.230579426152004885, -18.48807627814308674, -1.500000000000002220 ) ) ;
#28774=CARTESIAN_POINT ( 'NONE',  ( -19.33005188562793819, 9.364626179424670127, -1.500000000000002220 ) ) ;
#28776=LINE ( 'NONE', #21150, #48126 ) ;
#28777=CARTESIAN_POINT ( 'NONE',  ( -50.38822539166533687, -29.50249328176098729, 4.736241424693623081 ) ) ;
#28778=CARTESIAN_POINT ( 'NONE',  ( 6.015242202445381992, 21.98585358372262633, -1.500000000000002220 ) ) ;
#28781=CARTESIAN_POINT ( 'NONE',  ( -39.52287095715007581, -23.94994826722565406, -0.6494450866342755813 ) ) ;
#28782=DIRECTION ( 'NONE',  ( -3.773278334453080206E-23, 0.9999999999976377785, 2.173523156925979552E-06 ) ) ;
#28783=CARTESIAN_POINT ( 'NONE',  ( 7.431233518514567926, -18.57414813805618081, 11.49999999999999645 ) ) ;
#28786=CARTESIAN_POINT ( 'NONE',  ( -123.6228709571500701, -23.94994826722515668, -0.6494450866351689777 ) ) ;
#28788=ORIENTED_EDGE ( 'NONE', *, *, #8472, .T. ) ;
#28790=PLANE ( 'NONE',  #24765 ) ;
#28791=CARTESIAN_POINT ( 'NONE',  ( 14.84582651547613352, 15.88809324551894520, -1.500000000000002220 ) ) ;
#28793=CARTESIAN_POINT ( 'NONE',  ( 16.73968668634701729, 10.17700309559984717, -1.500000000000002220 ) ) ;
#28794=CARTESIAN_POINT ( 'NONE',  ( -99.71650429754699019, -25.16638005418298718, 6.902600843980934542 ) ) ;
#28795=ORIENTED_EDGE ( 'NONE', *, *, #91456, .F. ) ;
#28797=CARTESIAN_POINT ( 'NONE',  ( -60.62287095715006302, -24.15516710230295416, 10.28746687063727272 ) ) ;
#28799=CARTESIAN_POINT ( 'NONE',  ( -10.66544979547405347, 17.54311462378693420, 11.49999999999999645 ) ) ;
#28800=CARTESIAN_POINT ( 'NONE',  ( -93.62287095715005592, -29.50250243563736774, 8.947779886222139822 ) ) ;
#28804=CARTESIAN_POINT ( 'NONE',  ( -43.55620429048340014, -24.66019654487199020, 8.947790411086137041 ) ) ;
#28805=CARTESIAN_POINT ( 'NONE',  ( -110.6228709571500559, -29.50249982740957577, 7.747779886224967605 ) ) ;
#28808=EDGE_CURVE ( 'NONE', #75490, #71750, #96171, .T. ) ;
#28809=ORIENTED_EDGE ( 'NONE', *, *, #28043, .T. ) ;
#28811=AXIS2_PLACEMENT_3D ( 'NONE', #76760, #99599, #53464 ) ;
#28812=EDGE_CURVE ( 'NONE', #23301, #41495, #40382, .T. ) ;
#28813=B_SPLINE_CURVE_WITH_KNOTS ( 'NONE', 3,
 ( #10952, #42911, #4346, #20057 ),
 .UNSPECIFIED., .F., .F.,
 ( 4, 4 ),
 ( 0.000000000000000000, 9.999999999998897304E-05 ),
 .UNSPECIFIED. ) ;
#28814=CARTESIAN_POINT ( 'NONE',  ( -8.820007276677138464, 21.28423624206370945, 11.49999999999999645 ) ) ;
#28815=CARTESIAN_POINT ( 'NONE',  ( -18.67006117854901959, 13.05921059288911934, -1.500000000000002220 ) ) ;
#28816=CARTESIAN_POINT ( 'NONE',  ( -70.50669286463424612, -25.30458798213071248, 4.857674088053123285 ) ) ;
#28817=B_SPLINE_SURFACE_WITH_KNOTS ( 'NONE', 3, 3, ( 
 ( #67771, #60655, #83969, #20074 ),
 ( #53038, #37800, #29685, #97698 ),
 ( #99669, #35808, #6843, #30174 ),
 ( #20567, #89592, #36806, #12951 ),
 ( #13452, #76343, #68752, #52530 ),
 ( #43432, #74363, #83464, #51538 ),
 ( #44928, #59656, #6350, #75850 ) ),
 .UNSPECIFIED., .F., .F., .F.,
 ( 4, 3, 4 ),
 ( 4, 4 ),
 ( 0.0004766839783818343059, 0.1029713700210893729, 0.2054660560637969202 ),
 ( 0.6696643484175435201, 0.6709860548734745134 ),
 .UNSPECIFIED. ) ;
#28819=LINE ( 'NONE', #92697, #23618 ) ;
#28820=DIRECTION ( 'NONE',  ( 0.000000000000000000, -0.9999999999976377785, -2.173523156925979975E-06 ) ) ;
#28822=EDGE_CURVE ( 'NONE', #38937, #76505, #34144, .T. ) ;
#28823=CARTESIAN_POINT ( 'NONE',  ( -110.6235417928964040, -25.00158670708910336, 2.256160236439218814 ) ) ;
#28824=CARTESIAN_POINT ( 'NONE',  ( -17.52905966558703454, -13.16386835867055716, -1.500000000000002220 ) ) ;
#28827=CARTESIAN_POINT ( 'NONE',  ( -40.91416358624242378, -25.31564009351394162, 4.986335130569790053 ) ) ;
#28829=LINE ( 'NONE', #99809, #71154 ) ;
#28830=CARTESIAN_POINT ( 'NONE',  ( -60.91704107235849364, -25.28799268357646568, 6.054714359087114417 ) ) ;
#28831=VERTEX_POINT ( 'NONE', #49003 ) ;
#28833=CARTESIAN_POINT ( 'NONE',  ( 10.78675619948152864, -17.38023510967517637, 11.49999999999998934 ) ) ;
#28834=ORIENTED_EDGE ( 'NONE', *, *, #49725, .F. ) ;
#28835=ORIENTED_EDGE ( 'NONE', *, *, #98908, .T. ) ;
#28838=CARTESIAN_POINT ( 'NONE',  ( 22.66633601775066253, -4.223608244049824378, -1.500000000000002220 ) ) ;
#28839=CARTESIAN_POINT ( 'NONE',  ( -61.62757367957146926, -24.51314013834316441, 0.6176544820404165081 ) ) ;
#28840=CARTESIAN_POINT ( 'NONE',  ( -16.41926757845921614, -11.79510067912178606, -1.500000000000002220 ) ) ;
#28841=ORIENTED_EDGE ( 'NONE', *, *, #56811, .F. ) ;
#28842=CARTESIAN_POINT ( 'NONE',  ( -28.21458010398708893, -24.83337313992710449, 7.636915180611340226 ) ) ;
#28844=CARTESIAN_POINT ( 'NONE',  ( -40.84751817244628569, -25.30517900822009736, 5.505870246111851607 ) ) ;
#28846=B_SPLINE_CURVE_WITH_KNOTS ( 'NONE', 3,
 ( #28054, #12806, #75210, #98539 ),
 .UNSPECIFIED., .F., .F.,
 ( 4, 4 ),
 ( 0.000000000000000000, 0.0001000000000000028644 ),
 .UNSPECIFIED. ) ;
#28847=PLANE ( 'NONE',  #83714 ) ;
#28848=CARTESIAN_POINT ( 'NONE',  ( -99.50978007678189385, -24.51419770103158413, 9.386484678747176957 ) ) ;
#28849=CARTESIAN_POINT ( 'NONE',  ( 1.185105815240312888, -21.37944065014308848, 11.49999999999999645 ) ) ;
#28850=EDGE_LOOP ( 'NONE', ( #38805, #46342, #64899, #65008 ) ) ;
#28851=CARTESIAN_POINT ( 'NONE',  ( -77.55620429048339304, -23.48783264082478084, -1.443836473390065933 ) ) ;
#28852=ORIENTED_EDGE ( 'NONE', *, *, #15059, .T. ) ;
#28853=CARTESIAN_POINT ( 'NONE',  ( -19.59449498831206782, -6.737714454370689054, 11.49999999999998934 ) ) ;
#28860=ORIENTED_EDGE ( 'NONE', *, *, #1818, .F. ) ;
#28861=B_SPLINE_CURVE_WITH_KNOTS ( 'NONE', 3,
 ( #80917, #82407, #42382, #43860 ),
 .UNSPECIFIED., .F., .F.,
 ( 4, 4 ),
 ( 0.000000000000000000, 0.0001000000000000028644 ),
 .UNSPECIFIED. ) ;
#28862=CARTESIAN_POINT ( 'NONE',  ( -15.31302551872622075, -14.39686070098267479, -1.500000000000002220 ) ) ;
#28863=CARTESIAN_POINT ( 'NONE',  ( -21.26704322615652032, -5.532269525099344776, 11.49999999999999645 ) ) ;
#28864=CARTESIAN_POINT ( 'NONE',  ( -37.58093832661909772, -24.51419770103156637, 9.386484678747175181 ) ) ;
#28865=CARTESIAN_POINT ( 'NONE',  ( -21.23328875057882570, -7.520457577684837247, -1.500000000000002220 ) ) ;
#28866=CARTESIAN_POINT ( 'NONE',  ( -8.441512789788195192, 19.21024974253229800, -1.500000000000002220 ) ) ;
#28868=CARTESIAN_POINT ( 'NONE',  ( -72.62287095715004170, -23.94994826722515313, -0.6494450866351729745 ) ) ;
#28869=PLANE ( 'NONE',  #34602 ) ;
#28870=ORIENTED_EDGE ( 'NONE', *, *, #97028, .F. ) ;
#28871=ORIENTED_EDGE ( 'NONE', *, *, #24832, .F. ) ;
#28872=EDGE_LOOP ( 'NONE', ( #10899, #33909, #3032, #97501 ) ) ;
#28873=CARTESIAN_POINT ( 'NONE',  ( -124.6228709571500701, -23.47596703998600631, 11.44779298504227860 ) ) ;
#28874=CARTESIAN_POINT ( 'NONE',  ( 21.23773461148298836, -3.020459416520930862, -1.500000000000002220 ) ) ;
#28876=CARTESIAN_POINT ( 'NONE',  ( -105.5228709571500474, -24.91570333825769623, 8.075032458260368529 ) ) ;
#28877=ORIENTED_EDGE ( 'NONE', *, *, #99, .T. ) ;
#28878=CARTESIAN_POINT ( 'NONE',  ( -12.37649675270136918, 17.12833386298736471, -1.500000000000002220 ) ) ;
#28879=CARTESIAN_POINT ( 'NONE',  ( -52.62287095715004170, -23.47596703998600276, 11.44779298504227505 ) ) ;
#28880=CARTESIAN_POINT ( 'NONE',  ( -64.63158557479336253, -24.34968618360933590, 0.1864209137778785330 ) ) ;
#28881=CARTESIAN_POINT ( 'NONE',  ( -83.54431499582896947, -24.51419770103157347, 9.386484678747180510 ) ) ;
#28882=DIRECTION ( 'NONE',  ( -1.000000000000000000, -3.773278334444167608E-23, -8.201307833595939069E-29 ) ) ;
#28884=CARTESIAN_POINT ( 'NONE',  ( 21.80885565983754404, 3.581153529568561478, -1.500000000000002220 ) ) ;
#28885=CARTESIAN_POINT ( 'NONE',  ( -30.47961041733904608, -23.47593902323810156, -1.442222850822345581 ) ) ;
#28886=EDGE_CURVE ( 'NONE', #86024, #35233, #6263, .T. ) ;
#28887=CARTESIAN_POINT ( 'NONE',  ( -109.0882301073077514, -25.30385130285613471, 4.785588035035526211 ) ) ;
#28891=CARTESIAN_POINT ( 'NONE',  ( -16.21482014894483470, 10.69450053600103345, 11.49999999999998934 ) ) ;
#28892=CARTESIAN_POINT ( 'NONE',  ( -20.51402961445061734, 6.013860829077147585, 11.49999999999998934 ) ) ;
#28893=CARTESIAN_POINT ( 'NONE',  ( -66.62287095715005592, -23.48783264082478439, -1.443836473390067487 ) ) ;
#28894=CARTESIAN_POINT ( 'NONE',  ( -85.62287095715004170, -24.99156045073393173, 7.747789690856161648 ) ) ;
#28898=CARTESIAN_POINT ( 'NONE',  ( 0.4201012023153268271, 22.63755686032812164, -1.500000000000002220 ) ) ;
#28899=B_SPLINE_SURFACE_WITH_KNOTS ( 'NONE', 3, 3, ( 
 ( #91400, #14271, #20888, #60974 ),
 ( #13770, #13276, #36624, #75669 ),
 ( #67102, #30002, #6171, #21380 ),
 ( #7166, #52358, #75179, #45245 ),
 ( #6668, #38115, #51864, #5674 ),
 ( #91899, #22376, #53361, #21877 ),
 ( #5177, #76170, #76661, #61475 ) ),
 .UNSPECIFIED., .F., .F., .F.,
 ( 4, 3, 4 ),
 ( 4, 4 ),
 ( 0.0004766839783832283730, 0.1029713700210899835, 0.2054660560637967259 ),
 ( 0.9697406827104064764, 0.9712008438356087847 ),
 .UNSPECIFIED. ) ;
#28902=CARTESIAN_POINT ( 'NONE',  ( -97.58953762381671027, -24.64898659630367916, 1.056161002820388717 ) ) ;
#28903=CARTESIAN_POINT ( 'NONE',  ( 19.75791096855702733, 1.210928449428283038, 11.49999999999999645 ) ) ;
#28904=CARTESIAN_POINT ( 'NONE',  ( -82.62287095715004170, -24.33927499327854704, 9.819080762295817166 ) ) ;
#28905=CARTESIAN_POINT ( 'NONE',  ( -119.5895376238167103, -24.66019654487200086, 8.947790411086115725 ) ) ;
#28906=ORIENTED_EDGE ( 'NONE', *, *, #94937, .F. ) ;
#28908=CARTESIAN_POINT ( 'NONE',  ( -29.66447556523817397, -25.26026669889196086, 3.393817555207442105 ) ) ;
#28910=CARTESIAN_POINT ( 'NONE',  ( -2.642555958445479192, -21.45212208726272607, -1.500000000000002220 ) ) ;
#28911=CARTESIAN_POINT ( 'NONE',  ( -99.62287095715008434, -23.73907113216991860, -1.053371485793223927 ) ) ;
#28913=CARTESIAN_POINT ( 'NONE',  ( -66.52287095715003318, -24.35013146730204170, 9.818937971375099494 ) ) ;
#28915=CARTESIAN_POINT ( 'NONE',  ( -35.62287095715004170, -23.85196035786900737, -0.8779234886474999167 ) ) ;
#28916=CARTESIAN_POINT ( 'NONE',  ( -8.418173371947181849, -17.93405594323863284, 11.49999999999998934 ) ) ;
#28917=EDGE_LOOP ( 'NONE', ( #94655, #36368, #7535, #47069 ) ) ;
#28918=CARTESIAN_POINT ( 'NONE',  ( 15.61528876134825161, -13.05345633644532732, 11.49999999999999645 ) ) ;
#28920=DIRECTION ( 'NONE',  ( -3.773278334453079618E-23, 0.9999999999976377785, 2.173523156925979975E-06 ) ) ;
#28921=ORIENTED_EDGE ( 'NONE', *, *, #25756, .T. ) ;
#28922=CARTESIAN_POINT ( 'NONE',  ( -102.5930986047791151, -23.96169478059713498, 10.65365249895717881 ) ) ;
#28923=CARTESIAN_POINT ( 'NONE',  ( -111.6468792378192063, -25.29712067403330877, 4.332404411321261861 ) ) ;
#28924=FACE_OUTER_BOUND ( 'NONE', #235, .T. ) ;
#28927=CARTESIAN_POINT ( 'NONE',  ( -48.62287095715004881, -23.47596703998600276, 11.44779298504227505 ) ) ;
#28928=CARTESIAN_POINT ( 'NONE',  ( -16.72505113720834657, 11.10480813184383742, -1.500000000000002220 ) ) ;
#28929=PLANE ( 'NONE',  #40230 ) ;
#28933=VECTOR ( 'NONE', #87967, 1000.000000000000114 ) ;
#28934=CARTESIAN_POINT ( 'NONE',  ( 19.70479270790718829, 11.56945388388114360, 11.49999999999999645 ) ) ;
#28935=CARTESIAN_POINT ( 'NONE',  ( -30.47287095715005734, -24.90571414232896785, 1.932341227645357318 ) ) ;
#28937=DIRECTION ( 'NONE',  ( 0.000000000000000000, -0.9999999999976377785, -2.173523156925979975E-06 ) ) ;
#28941=CARTESIAN_POINT ( 'NONE',  ( -66.52287095715006160, -29.50250243563736774, 8.947779886222143375 ) ) ;
#28942=PLANE ( 'NONE',  #69555 ) ;
#28944=CARTESIAN_POINT ( 'NONE',  ( 10.94010344783756672, -17.16519937159427656, -1.500000000000002220 ) ) ;
#28945=VERTEX_POINT ( 'NONE', #78925 ) ;
#28946=EDGE_CURVE ( 'NONE', #37803, #82227, #19033, .T. ) ;
#28947=CARTESIAN_POINT ( 'NONE',  ( 4.748521865011817944, 22.44708532425888592, -1.500000000000002220 ) ) ;
#28948=CARTESIAN_POINT ( 'NONE',  ( 5.514125806255895004E-17, -29.50248528299875161, 1.056150778585261296 ) ) ;
#28949=EDGE_LOOP ( 'NONE', ( #68400, #18381, #96037, #53203 ) ) ;
#28950=PLANE ( 'NONE',  #36403 ) ;
#28951=CARTESIAN_POINT ( 'NONE',  ( -77.58808754410065944, -24.35071581493544102, 9.817618358456021710 ) ) ;
#28953=CARTESIAN_POINT ( 'NONE',  ( -18.72683625574626376, -10.08736549105613278, 11.49999999999999645 ) ) ;
#28955=ORIENTED_EDGE ( 'NONE', *, *, #21794, .T. ) ;
#28956=CARTESIAN_POINT ( 'NONE',  ( -10.56713949322891999, -19.48831581008217384, 11.49999999999998934 ) ) ;
#28957=CARTESIAN_POINT ( 'NONE',  ( -18.82610421443283499, -8.410905081555696938, -1.500000000000002220 ) ) ;
#28960=CARTESIAN_POINT ( 'NONE',  ( -64.52287095715006160, -23.47596703998600631, 11.44779298504228926 ) ) ;
#28961=CARTESIAN_POINT ( 'NONE',  ( -39.51069479889651603, -25.17639606163672283, 3.166201134751521540 ) ) ;
#28962=ORIENTED_EDGE ( 'NONE', *, *, #27688, .F. ) ;
#28964=VERTEX_POINT ( 'NONE', #10930 ) ;
#28965=LINE ( 'NONE', #90866, #63249 ) ;
#28966=CARTESIAN_POINT ( 'NONE',  ( -75.62287095715005592, -23.84081130438200802, 10.88220057463249013 ) ) ;
#28967=CARTESIAN_POINT ( 'NONE',  ( -83.52287095715006160, -23.47593901973090524, -1.443836447538996648 ) ) ;
#28968=CARTESIAN_POINT ( 'NONE',  ( 20.09396958936853395, 5.161349618257207617, -1.500000000000002220 ) ) ;
#28969=CARTESIAN_POINT ( 'NONE',  ( -14.02725853290852243, 16.66567569088042688, 11.49999999999999645 ) ) ;
#28970=CARTESIAN_POINT ( 'NONE',  ( -35.62287095715005592, -29.50249982740957577, 7.747779886224967605 ) ) ;
#28972=CARTESIAN_POINT ( 'NONE',  ( -115.5868014046007204, -25.00158670708910691, 2.256160236439219258 ) ) ;
#28973=CARTESIAN_POINT ( 'NONE',  ( -22.41777205227948855, 0.6913007675000180097, -1.500000000000002220 ) ) ;
#28978=DIRECTION ( 'NONE',  ( -3.773278334453079618E-23, 0.9999999999976377785, 2.173523156925979975E-06 ) ) ;
#28979=CARTESIAN_POINT ( 'NONE',  ( -50.70524595056228634, -25.11617103263561290, 2.864784757501792622 ) ) ;
#28980=ORIENTED_EDGE ( 'NONE', *, *, #99098, .F. ) ;
#28981=AXIS2_PLACEMENT_3D ( 'NONE', #56411, #43047, #87330 ) ;
#28982=ORIENTED_EDGE ( 'NONE', *, *, #20555, .T. ) ;
#28983=CARTESIAN_POINT ( 'NONE',  ( -99.30784767537812741, -25.27538107857485272, 5.993649293344923912 ) ) ;
#28984=EDGE_CURVE ( 'NONE', #61594, #73153, #20814, .T. ) ;
#28985=EDGE_LOOP ( 'NONE', ( #19993, #53682, #1806, #84738 ) ) ;
#28986=CARTESIAN_POINT ( 'NONE',  ( -12.14505723179402530, 17.47690347785001919, -1.500000000000002220 ) ) ;
#28989=CARTESIAN_POINT ( 'NONE',  ( -9.798014431990228701, 18.61115389415964572, 11.49999999999998934 ) ) ;
#28991=CARTESIAN_POINT ( 'NONE',  ( 16.14549698687068968, 15.95341496147077720, 11.49999999999998934 ) ) ;
#28994=DIRECTION ( 'NONE',  ( -3.773278334444167608E-23, 1.000000000000000000, 0.000000000000000000 ) ) ;
#28995=CARTESIAN_POINT ( 'NONE',  ( -21.18249553426131015, -5.656070447573528170, -1.500000000000002220 ) ) ;
#28996=CARTESIAN_POINT ( 'NONE',  ( -117.6228709571500559, -29.50250786944525672, 11.44777988621622811 ) ) ;
#28997=ORIENTED_EDGE ( 'NONE', *, *, #9337, .F. ) ;
#28998=CARTESIAN_POINT ( 'NONE',  ( -122.5564250028337767, -23.73791477778912551, 11.05961554403169878 ) ) ;
#28999=LINE ( 'NONE', #21868, #88637 ) ;
#29000=CARTESIAN_POINT ( 'NONE',  ( -41.62287095715007013, -23.96127896941631619, -0.6493128931037902563 ) ) ;
#29002=CARTESIAN_POINT ( 'NONE',  ( -3.310264809446246570, -21.00426241492911927, 11.49999999999998934 ) ) ;
#29003=CARTESIAN_POINT ( 'NONE',  ( -119.6228709571500559, -29.50247984919015209, -1.443849546365046699 ) ) ;
#29005=EDGE_CURVE ( 'NONE', #35855, #16750, #58121, .T. ) ;
#29006=CARTESIAN_POINT ( 'NONE',  ( -85.54293262885111915, -24.73486907724917927, 1.287355809206964796 ) ) ;
#29010=CARTESIAN_POINT ( 'NONE',  ( -117.5903086160344344, -24.15620529776629510, 10.23563542870659582 ) ) ;
#29012=CARTESIAN_POINT ( 'NONE',  ( -119.5895376238167245, -24.65952944569306027, 1.056160979905711894 ) ) ;
#29013=CARTESIAN_POINT ( 'NONE',  ( 16.91694316922610497, -9.995573847407506207, 11.49999999999999645 ) ) ;
#29014=CARTESIAN_POINT ( 'NONE',  ( -75.62287095715004170, -24.99156045073392818, 7.747789690856161648 ) ) ;
#29017=CARTESIAN_POINT ( 'NONE',  ( -88.63497858377701277, -23.96169478059713853, 10.65365249895717703 ) ) ;
#29019=CARTESIAN_POINT ( 'NONE',  ( -100.6347018612127613, -25.03409664067351059, 7.557395711288017459 ) ) ;
#29020=CARTESIAN_POINT ( 'NONE',  ( -31.62287095715005236, -23.72747288104441665, -1.053458166803663554 ) ) ;
#29021=CARTESIAN_POINT ( 'NONE',  ( -40.62287095715005592, -24.82576562982392687, 8.398263435472978600 ) ) ;
#29022=CARTESIAN_POINT ( 'NONE',  ( -18.24397684793207830, 7.494555614300850266, 11.49999999999998934 ) ) ;
#29023=ORIENTED_EDGE ( 'NONE', *, *, #28466, .T. ) ;
#29025=CARTESIAN_POINT ( 'NONE',  ( -126.6228709571500559, -24.64965695001469825, 8.947790433994173398 ) ) ;
#29027=ORIENTED_EDGE ( 'NONE', *, *, #16253, .T. ) ;
#29028=CARTESIAN_POINT ( 'NONE',  ( -107.5562042904834215, -24.64965694238575011, 8.947790433994189385 ) ) ;
#29030=CARTESIAN_POINT ( 'NONE',  ( -55.62594774802067121, -24.92564183028978775, 1.928384488918253092 ) ) ;
#29032=CARTESIAN_POINT ( 'NONE',  ( -121.5228709571500616, -24.65952944569305316, 1.056160979905705899 ) ) ;
#29034=CARTESIAN_POINT ( 'NONE',  ( -99.62287095715004170, -24.66019654487199730, 8.947790411086122830 ) ) ;
#29035=CARTESIAN_POINT ( 'NONE',  ( -107.5179598396476024, -23.96119346886881729, -0.6495511937831858207 ) ) ;
#29036=CARTESIAN_POINT ( 'NONE',  ( 13.87436705529610492, 14.39054836566213780, 11.49999999999998934 ) ) ;
#29037=EDGE_CURVE ( 'NONE', #65549, #25965, #37264, .T. ) ;
#29038=CARTESIAN_POINT ( 'NONE',  ( -127.6228709571500559, -23.72747288104441665, -1.053458166803660445 ) ) ;
#29039=CARTESIAN_POINT ( 'NONE',  ( -0.0004629052523845373149, -23.04400732772759142, 4.713857633697502436 ) ) ;
#29040=ORIENTED_EDGE ( 'NONE', *, *, #22177, .F. ) ;
#29045=CARTESIAN_POINT ( 'NONE',  ( -119.5526355611971638, -24.65952944569305672, 1.056160979905715003 ) ) ;
#29047=CARTESIAN_POINT ( 'NONE',  ( -28.58953762381674224, -24.49351198072915281, 1.056161665704728136 ) ) ;
#29048=CARTESIAN_POINT ( 'NONE',  ( -39.59380959696974855, -24.15543982623906416, -0.2315651400026677575 ) ) ;
#29049=VECTOR ( 'NONE', #79112, 1000.000000000000114 ) ;
#29050=EDGE_CURVE ( 'NONE', #21474, #37981, #1433, .T. ) ;
#29052=CARTESIAN_POINT ( 'NONE',  ( -51.04357394935764347, -25.26280107025014132, 4.940878043609458814 ) ) ;
#29054=CARTESIAN_POINT ( 'NONE',  ( -34.62287095715006302, -24.51283580621363711, 0.6167428607019808107 ) ) ;
#29057=CARTESIAN_POINT ( 'NONE',  ( -18.19507518397214341, 8.946258903265221107, 11.49999999999998934 ) ) ;
#29058=CARTESIAN_POINT ( 'NONE',  ( -122.5222492194006207, -23.48783264082477373, -1.443836473390087471 ) ) ;
#29060=CARTESIAN_POINT ( 'NONE',  ( -49.62287095715005592, -24.65952944569304250, 1.056160979905693020 ) ) ;
#29061=ADVANCED_FACE ( 'NONE', ( #59113 ), #35276, .T. ) ;
#29062=DIRECTION ( 'NONE',  ( -3.773278334453079030E-23, 0.9999999999976377785, 2.173523156925979128E-06 ) ) ;
#29063=ORIENTED_EDGE ( 'NONE', *, *, #24091, .T. ) ;
#29064=CARTESIAN_POINT ( 'NONE',  ( -78.52287095715004739, -24.66019654487199375, 8.947790411086119278 ) ) ;
#29066=CARTESIAN_POINT ( 'NONE',  ( -1.723993941171178879, -19.98520929721398431, -1.500000000000002220 ) ) ;
#29067=CARTESIAN_POINT ( 'NONE',  ( 5.994809752082427501, 20.21905721239408393, 11.49999999999999645 ) ) ;
#29069=CARTESIAN_POINT ( 'NONE',  ( -70.62545108457702270, -24.92592662359561118, 8.075495903017998245 ) ) ;
#29070=CARTESIAN_POINT ( 'NONE',  ( -14.46940225681120396, -16.66540133702554272, -1.500000000000002220 ) ) ;
#29071=B_SPLINE_CURVE_WITH_KNOTS ( 'NONE', 3,
 ( #46323, #92983, #8262, #77251 ),
 .UNSPECIFIED., .F., .F.,
 ( 4, 4 ),
 ( 6.938893903907228378E-18, 0.0001000000000000167422 ),
 .UNSPECIFIED. ) ;
#29072=CARTESIAN_POINT ( 'NONE',  ( -13.21525772315781388, 15.71049578022273785, 11.49999999999998934 ) ) ;
#29076=VERTEX_POINT ( 'NONE', #20522 ) ;
#29077=LINE ( 'NONE', #13346, #839 ) ;
#29079=CARTESIAN_POINT ( 'NONE',  ( -29.55620429048340370, -23.39163958139442556, -1.443836129118754696 ) ) ;
#29080=ORIENTED_EDGE ( 'NONE', *, *, #53805, .F. ) ;
#29081=ORIENTED_EDGE ( 'NONE', *, *, #81844, .F. ) ;
#29082=DIRECTION ( 'NONE',  ( -1.000000000000000000, -3.773278334444166432E-23, -8.201307841325785021E-29 ) ) ;
#29084=CARTESIAN_POINT ( 'NONE',  ( -76.53952647890686478, -24.65952944569303895, 1.056160979905700570 ) ) ;
#29085=CARTESIAN_POINT ( 'NONE',  ( 7.647619880454145758, 19.11525441646967849, -1.500000000000002220 ) ) ;
#29086=CARTESIAN_POINT ( 'NONE',  ( -13.01863397230089170, 17.21462230531794901, 11.49999999999999645 ) ) ;
#29088=CARTESIAN_POINT ( 'NONE',  ( -99.36517007105946675, -25.30168654129753136, 4.687587830358475038 ) ) ;
#29089=DIRECTION ( 'NONE',  ( 0.000000000000000000, 2.173523156925980399E-06, -0.9999999999976378895 ) ) ;
#29090=CARTESIAN_POINT ( 'NONE',  ( 17.53502452033532677, 13.85421504792973479, 11.49999999999998934 ) ) ;
#29091=CARTESIAN_POINT ( 'NONE',  ( -48.52287095715006160, -23.48786465467241769, 11.44779295918255002 ) ) ;
#29093=ORIENTED_EDGE ( 'NONE', *, *, #73110, .F. ) ;
#29094=CARTESIAN_POINT ( 'NONE',  ( -50.55620429048339304, -25.00182538069145011, 7.747789668545099317 ) ) ;
#29096=CARTESIAN_POINT ( 'NONE',  ( 20.36350155627077640, -4.707376482769925374, -1.500000000000002220 ) ) ;
#29099=CARTESIAN_POINT ( 'NONE',  ( -39.44687923781921057, -25.28830591450888221, 4.188173661249233959 ) ) ;
#29102=EDGE_CURVE ( 'NONE', #64035, #40077, #98272, .T. ) ;
#29103=CARTESIAN_POINT ( 'NONE',  ( -50.49632248188068928, -25.30259173606348000, 4.732524148509932083 ) ) ;
#29104=CARTESIAN_POINT ( 'NONE',  ( 17.50165659415881336, 11.77592616506222711, -1.500000000000002220 ) ) ;
#29105=EDGE_LOOP ( 'NONE', ( #7739, #67498, #100047, #47308 ) ) ;
#29106=CARTESIAN_POINT ( 'NONE',  ( -117.6260434375350172, -24.15543982623907837, -0.2315651400026547124 ) ) ;
#29107=CARTESIAN_POINT ( 'NONE',  ( -100.1979988280279201, -25.12215671659214777, 7.085055038744845213 ) ) ;
#29108=CARTESIAN_POINT ( 'NONE',  ( 20.45693200876408469, 7.529271608661172621, -1.500000000000002220 ) ) ;
#29113=CARTESIAN_POINT ( 'NONE',  ( 18.07971092720299922, 12.08445254275838465, -1.500000000000002220 ) ) ;
#29114=CARTESIAN_POINT ( 'NONE',  ( -71.68214140181162009, -25.24674281957223343, 5.908703891276553044 ) ) ;
#29115=CARTESIAN_POINT ( 'NONE',  ( -22.28969446433750434, -1.297463027894488086, 11.49999999999999645 ) ) ;
#29117=DIRECTION ( 'NONE',  ( 0.000000000000000000, 0.9999999999976377785, 2.173523156925979975E-06 ) ) ;
#29119=CARTESIAN_POINT ( 'NONE',  ( -106.6228709571500559, -29.50250243563736774, 8.947779886222136270 ) ) ;
#29120=ORIENTED_EDGE ( 'NONE', *, *, #3081, .T. ) ;
#29122=ORIENTED_EDGE ( 'NONE', *, *, #3628, .T. ) ;
#29124=ORIENTED_EDGE ( 'NONE', *, *, #15511, .T. ) ;
#29126=CARTESIAN_POINT ( 'NONE',  ( -82.62287095715005592, -24.64898659630367916, 1.056161002820826145 ) ) ;
#29127=CARTESIAN_POINT ( 'NONE',  ( -87.62287095715004170, -29.50247984919015209, -1.443849546365051806 ) ) ;
#29130=EDGE_CURVE ( 'NONE', #15603, #46174, #69162, .T. ) ;
#29132=CARTESIAN_POINT ( 'NONE',  ( -17.02366064725396555, -9.230830265533395362, -1.500000000000002220 ) ) ;
#29136=CARTESIAN_POINT ( 'NONE',  ( 13.32768686175602646, -14.16729652289716057, 11.49999999999999645 ) ) ;
#29137=CARTESIAN_POINT ( 'NONE',  ( -81.62287095715008434, -23.47596703998600631, 11.44779298504227860 ) ) ;
#29140=DIRECTION ( 'NONE',  ( 0.000000000000000000, 0.9999999999976377785, 2.173523156925979128E-06 ) ) ;
#29142=CARTESIAN_POINT ( 'NONE',  ( -109.8650282762807393, -29.50249556043354460, 5.784618828537300139 ) ) ;
#29143=ADVANCED_FACE ( 'NONE', ( #13908 ), #82920, .T. ) ;
#29144=CARTESIAN_POINT ( 'NONE',  ( -97.26334014122947735, -23.47596703998600631, 11.44779298504227860 ) ) ;
#29145=CARTESIAN_POINT ( 'NONE',  ( 5.117700956428186565, 18.95590836763280862, -1.500000000000002220 ) ) ;
#29146=CARTESIAN_POINT ( 'NONE',  ( -37.58953762381673869, -24.64898659630367206, 1.056161002820379169 ) ) ;
#29149=CARTESIAN_POINT ( 'NONE',  ( 14.33184905138074683, -16.10332302735202958, -1.500000000000002220 ) ) ;
#29150=LINE ( 'NONE', #59618, #64160 ) ;
#29152=CARTESIAN_POINT ( 'NONE',  ( -40.66404017723625941, -23.85016227208580730, -0.8807180028928393023 ) ) ;
#29153=CARTESIAN_POINT ( 'NONE',  ( -99.52764846858842418, -25.18439489159435496, 3.999772444794112314 ) ) ;
#29154=CARTESIAN_POINT ( 'NONE',  ( -22.87025945403008365, 2.249016246415321163, -1.500000000000002220 ) ) ;
#29155=B_SPLINE_CURVE_WITH_KNOTS ( 'NONE', 3,
 ( #83914, #51979, #59102, #74313 ),
 .UNSPECIFIED., .F., .F.,
 ( 4, 4 ),
 ( 0.9704789197191771022, 0.9794853509912926359 ),
 .UNSPECIFIED. ) ;
#29158=CARTESIAN_POINT ( 'NONE',  ( -49.50018282194935182, -25.18370859199909972, 3.285367768258824483 ) ) ;
#29159=CARTESIAN_POINT ( 'NONE',  ( -15.75104486599040321, 12.61009050114280861, 11.49999999999999645 ) ) ;
#29160=CARTESIAN_POINT ( 'NONE',  ( -101.5228709571500758, -24.64898659630368627, 1.056161002820829697 ) ) ;
#29163=CARTESIAN_POINT ( 'NONE',  ( -50.62287095715005592, -23.47596703998600631, 11.44779298504227505 ) ) ;
#29165=CARTESIAN_POINT ( 'NONE',  ( 8.615496892348360802, 17.92367856960711947, -1.500000000000002220 ) ) ;
#29168=CARTESIAN_POINT ( 'NONE',  ( 19.18382676146983457, -4.683391092530263755, -1.500000000000002220 ) ) ;
#29169=CARTESIAN_POINT ( 'NONE',  ( -126.5909419807629490, -23.48786465467241769, 11.44779295918253759 ) ) ;
#29171=CARTESIAN_POINT ( 'NONE',  ( -37.52287095715008292, -23.48783264083359512, -1.443836473376374885 ) ) ;
#29172=CARTESIAN_POINT ( 'NONE',  ( 1.453578435135240321, -20.60874541997745268, 11.49999999999999645 ) ) ;
#29173=CARTESIAN_POINT ( 'NONE',  ( -111.5228709571500616, -24.64965694238407323, 8.947790433994192938 ) ) ;
#29174=B_SPLINE_CURVE_WITH_KNOTS ( 'NONE', 3,
 ( #62711, #100224, #15502, #55093, #39850, #46469 ),
 .UNSPECIFIED., .F., .F.,
 ( 4, 2, 4 ),
 ( 1.570755371634072366E-05, 0.001396183895866090138, 0.002776660238015839482 ),
 .UNSPECIFIED. ) ;
#29177=DIRECTION ( 'NONE',  ( 3.773278334444166432E-23, -1.000000000000000000, 0.000000000000000000 ) ) ;
#29178=CARTESIAN_POINT ( 'NONE',  ( -9.471985145535571249, 20.67137392225973258, 11.49999999999999645 ) ) ;
#29179=VERTEX_POINT ( 'NONE', #43388 ) ;
#29180=CARTESIAN_POINT ( 'NONE',  ( -46.62287095715004881, -23.48786465467241058, 11.44779295918255180 ) ) ;
#29184=CARTESIAN_POINT ( 'NONE',  ( -8.513533612778267923, 18.29693335657625042, -1.500000000000002220 ) ) ;
#29185=PLANE ( 'NONE',  #64667 ) ;
#29186=ADVANCED_FACE ( 'NONE', ( #5806 ), #61614, .T. ) ;
#29189=ORIENTED_EDGE ( 'NONE', *, *, #49224, .F. ) ;
#29190=EDGE_CURVE ( 'NONE', #76875, #48556, #52284, .T. ) ;
#29191=EDGE_LOOP ( 'NONE', ( #85723, #57669, #26496, #83490 ) ) ;
#29193=B_SPLINE_CURVE_WITH_KNOTS ( 'NONE', 3,
 ( #24511, #79799, #55480, #32628 ),
 .UNSPECIFIED., .F., .F.,
 ( 4, 4 ),
 ( 0.000000000000000000, 9.999999999993347544E-05 ),
 .UNSPECIFIED. ) ;
#29194=CARTESIAN_POINT ( 'NONE',  ( 22.22072617242880455, -5.352622178732230118, 11.49999999999998934 ) ) ;
#29195=CARTESIAN_POINT ( 'NONE',  ( -29.62374991441511440, -24.58397407072015639, 1.056161296257513982 ) ) ;
#29197=AXIS2_PLACEMENT_3D ( 'NONE', #85637, #85134, #1417 ) ;
#29198=CARTESIAN_POINT ( 'NONE',  ( -20.54952838774410750, 6.582847151591199264, -1.500000000000002220 ) ) ;
#29199=DIRECTION ( 'NONE',  ( -3.773278334453079030E-23, 0.9999999999976377785, 2.173523156925979128E-06 ) ) ;
#29201=CARTESIAN_POINT ( 'NONE',  ( 16.93931825803137414, 14.88162037096512158, 11.49999999999999645 ) ) ;
#29204=CARTESIAN_POINT ( 'NONE',  ( -43.52287095715008292, -24.51283580621452529, 0.6167428607045876143 ) ) ;
#29205=CARTESIAN_POINT ( 'NONE',  ( 19.49364837986538745, 10.19379059548657551, -1.500000000000002220 ) ) ;
#29207=CARTESIAN_POINT ( 'NONE',  ( -105.5090414728886117, -24.83644354573579349, 8.397322867130096569 ) ) ;
#29208=CARTESIAN_POINT ( 'NONE',  ( -41.16467076663393243, -25.29087073963488663, 3.014415608521074486 ) ) ;
#29210=CARTESIAN_POINT ( 'NONE',  ( -73.55620429048340725, -23.47593901973091235, -1.443836447539006196 ) ) ;
#29211=CARTESIAN_POINT ( 'NONE',  ( -90.54765750514137324, -24.52399227489126687, 9.353111116836531735 ) ) ;
#29213=DIRECTION ( 'NONE',  ( 1.000000000000000000, 3.773278334444166432E-23, 8.201307841325785021E-29 ) ) ;
#29214=VERTEX_POINT ( 'NONE', #32135 ) ;
#29215=ORIENTED_EDGE ( 'NONE', *, *, #95018, .F. ) ;
#29216=CARTESIAN_POINT ( 'NONE',  ( -49.27764846858840997, -25.26180677598144086, 6.145204968850301874 ) ) ;
#29218=CARTESIAN_POINT ( 'NONE',  ( -57.55991777488805639, -23.73766607897670866, -1.055555164236458454 ) ) ;
#29219=CARTESIAN_POINT ( 'NONE',  ( -13.80512455850298714, -15.04058748057734896, -1.500000000000002220 ) ) ;
#29220=EDGE_LOOP ( 'NONE', ( #87765, #98833, #29826, #37258 ) ) ;
#29224=CARTESIAN_POINT ( 'NONE',  ( -25.53323730411857895, -24.91674856234845592, 5.128073852591860771 ) ) ;
#29225=ORIENTED_EDGE ( 'NONE', *, *, #10549, .T. ) ;
#29227=DIRECTION ( 'NONE',  ( 0.000000000000000000, -2.173523156925979552E-06, 0.9999999999976378895 ) ) ;
#29228=CARTESIAN_POINT ( 'NONE',  ( 7.312689604342500260, -19.48077458720139532, 11.49999999999998934 ) ) ;
#29231=ORIENTED_EDGE ( 'NONE', *, *, #60045, .F. ) ;
#29232=DIRECTION ( 'NONE',  ( 0.000000000000000000, 0.9999999999976377785, 2.173523156925979128E-06 ) ) ;
#29234=ORIENTED_EDGE ( 'NONE', *, *, #31399, .T. ) ;
#29235=FACE_OUTER_BOUND ( 'NONE', #19389, .T. ) ;
#29236=CARTESIAN_POINT ( 'NONE',  ( -120.6228709571500417, -23.47593901973091235, -1.443836447538997536 ) ) ;
#29237=CARTESIAN_POINT ( 'NONE',  ( -80.55620429048339304, -25.00158670708909625, 2.256160236439166855 ) ) ;
#29238=CARTESIAN_POINT ( 'NONE',  ( -82.52287095715006160, -29.50247984919015209, -1.443849546365053582 ) ) ;
#29239=CARTESIAN_POINT ( 'NONE',  ( -4.051365815588555463, -21.74199345402511696, 11.49999999999999645 ) ) ;
#29240=VERTEX_POINT ( 'NONE', #54483 ) ;
#29242=CARTESIAN_POINT ( 'NONE',  ( 8.854694546379761277, 20.84150027139232364, 11.49999999999998934 ) ) ;
#29243=CARTESIAN_POINT ( 'NONE',  ( -115.5868009550897000, -25.00182538069147142, 7.747789668545041586 ) ) ;
#29244=ORIENTED_EDGE ( 'NONE', *, *, #44154, .T. ) ;
#29248=EDGE_CURVE ( 'NONE', #75484, #27205, #11127, .T. ) ;
#29249=CARTESIAN_POINT ( 'NONE',  ( -16.19606052442943067, -11.93128464602566474, -1.500000000000002220 ) ) ;
#29252=EDGE_CURVE ( 'NONE', #21619, #86369, #151, .T. ) ;
#29253=CARTESIAN_POINT ( 'NONE',  ( -40.09822460666767086, -25.29345413520112018, 5.519450583125844467 ) ) ;
#29254=CARTESIAN_POINT ( 'NONE',  ( 14.50327815619135308, -17.01817589256642194, -1.500000000000002220 ) ) ;
#29256=ORIENTED_EDGE ( 'NONE', *, *, #30517, .T. ) ;
#29257=ORIENTED_EDGE ( 'NONE', *, *, #25712, .F. ) ;
#29260=CARTESIAN_POINT ( 'NONE',  ( -26.36280243631113507, -24.64751895363565737, 2.181899612272915956 ) ) ;
#29261=EDGE_CURVE ( 'NONE', #10349, #55337, #84922, .T. ) ;
#29265=VECTOR ( 'NONE', #5678, 1000.000000000000114 ) ;
#29266=CARTESIAN_POINT ( 'NONE',  ( 14.28107258077893604, -13.35224110012613963, -1.500000000000002220 ) ) ;
#29267=DIRECTION ( 'NONE',  ( -3.773278334453079618E-23, 0.9999999999976377785, 2.173523156925979975E-06 ) ) ;
#29268=AXIS2_PLACEMENT_3D ( 'NONE', #99466, #60934, #69543 ) ;
#29269=ADVANCED_FACE ( 'NONE', ( #76301 ), #70705, .T. ) ;
#29270=CARTESIAN_POINT ( 'NONE',  ( -20.40864349294084334, -6.676163967499375573, 11.49999999999998934 ) ) ;
#29271=CARTESIAN_POINT ( 'NONE',  ( -25.74893805332498076, -24.92775014605368256, 3.231001575389719882 ) ) ;
#29272=FACE_OUTER_BOUND ( 'NONE', #86641, .T. ) ;
#29274=CARTESIAN_POINT ( 'NONE',  ( 22.73759373355791169, -1.750760473330008171, -1.500000000000002220 ) ) ;
#29275=AXIS2_PLACEMENT_3D ( 'NONE', #27287, #97782, #66364 ) ;
#29277=CARTESIAN_POINT ( 'NONE',  ( -96.58867564644825165, -24.35071581493543391, 9.817618358456023486 ) ) ;
#29279=CARTESIAN_POINT ( 'NONE',  ( -4.495603250223349612, -19.44740727768710187, 11.49999999999999645 ) ) ;
#29280=CARTESIAN_POINT ( 'NONE',  ( -64.52287095715006160, -24.64898659630528854, 1.056161002820822592 ) ) ;
#29281=CARTESIAN_POINT ( 'NONE',  ( -74.50753224588216028, -24.15620529776628800, 10.23563542870659937 ) ) ;
#29286=DIRECTION ( 'NONE',  ( -1.000000000000000000, -3.773278334444167608E-23, -8.201307833595939069E-29 ) ) ;
#29287=CARTESIAN_POINT ( 'NONE',  ( -18.42844947050907578, 11.51566461966115540, -1.500000000000002220 ) ) ;
#29289=CARTESIAN_POINT ( 'NONE',  ( 12.01011565470214393, -15.49198969801113890, -1.500000000000002220 ) ) ;
#29290=FACE_OUTER_BOUND ( 'NONE', #76033, .T. ) ;
#29292=EDGE_LOOP ( 'NONE', ( #97479, #70769, #79988, #56412 ) ) ;
#29293=CARTESIAN_POINT ( 'NONE',  ( -108.8968792378191779, -25.11711062963908603, 7.140618811323130366 ) ) ;
#29295=CARTESIAN_POINT ( 'NONE',  ( -15.50425215161893355, 13.37805140191733777, 11.49999999999999645 ) ) ;
#29297=ADVANCED_FACE ( 'NONE', ( #53500 ), #46366, .T. ) ;
#29300=CARTESIAN_POINT ( 'NONE',  ( -109.4921708791334396, -25.30340751872594396, 4.738595968073344267 ) ) ;
#29301=CARTESIAN_POINT ( 'NONE',  ( -40.06853693287165186, -25.28892436075654970, 3.358277935517027135 ) ) ;
#29308=CARTESIAN_POINT ( 'NONE',  ( -0.3492834940180428727, 22.98956000712751546, 11.49999999999999645 ) ) ;
#29309=CARTESIAN_POINT ( 'NONE',  ( -22.16177213047534877, -5.259615592301647879, -1.500000000000002220 ) ) ;
#29310=CARTESIAN_POINT ( 'NONE',  ( -34.52287095715006160, -23.47596703998600631, 11.44779298504229459 ) ) ;
#29312=PLANE ( 'NONE',  #87341 ) ;
#29313=CARTESIAN_POINT ( 'NONE',  ( -115.5228709571500332, -23.85196035786900026, -0.8779234886475116850 ) ) ;
#29314=CARTESIAN_POINT ( 'NONE',  ( -69.62287095715005592, -24.64898659630528854, 1.056161002820824368 ) ) ;
#29317=CARTESIAN_POINT ( 'NONE',  ( 15.10893391618534665, -15.86458014800626692, 11.49999999999998934 ) ) ;
#29318=CARTESIAN_POINT ( 'NONE',  ( -97.62287095715005592, -29.50250243563736774, 8.947779886222138046 ) ) ;
#29320=CARTESIAN_POINT ( 'NONE',  ( -40.73160982624488469, -25.31552648564060348, 5.045570495695059776 ) ) ;
#29321=CARTESIAN_POINT ( 'NONE',  ( -125.5895376238167529, -24.99156044556120904, 7.747789690856343725 ) ) ;
#29322=CARTESIAN_POINT ( 'NONE',  ( -117.6228709571500701, -24.50216790748100237, 0.6166512839513771382 ) ) ;
#29325=CARTESIAN_POINT ( 'NONE',  ( 19.09590870110849181, 7.302211495713927469, 11.49999999999998934 ) ) ;
#29326=ORIENTED_EDGE ( 'NONE', *, *, #99941, .F. ) ;
#29330=EDGE_CURVE ( 'NONE', #71528, #51268, #93027, .T. ) ;
#29331=CARTESIAN_POINT ( 'NONE',  ( 6.753845092018655016, 22.03294598498517232, 11.49999999999998934 ) ) ;
#29332=CARTESIAN_POINT ( 'NONE',  ( -61.64837733756440485, -23.73766607897669800, -1.055555164236459120 ) ) ;
#29333=CARTESIAN_POINT ( 'NONE',  ( -9.470923242388245455, -17.85692771776473364, -1.500000000000002220 ) ) ;
#29334=EDGE_LOOP ( 'NONE', ( #4641, #96936, #89489, #24614 ) ) ;
#29335=CARTESIAN_POINT ( 'NONE',  ( -35.62287095715005592, -25.00182538069145011, 7.747789668545097541 ) ) ;
#29336=DIRECTION ( 'NONE',  ( -3.773278334453079030E-23, 0.9999999999976377785, 2.173523156925979128E-06 ) ) ;
#29337=VECTOR ( 'NONE', #11935, 1000.000000000000227 ) ;
#29338=PLANE ( 'NONE',  #82127 ) ;
#29339=CARTESIAN_POINT ( 'NONE',  ( -99.59615874627706944, -23.73791477778911840, 11.05961554403170410 ) ) ;
#29340=CARTESIAN_POINT ( 'NONE',  ( 15.25824911148008844, 15.06768998368162471, 11.49999999999999645 ) ) ;
#29341=EDGE_LOOP ( 'NONE', ( #2312, #99931, #67838, #76522 ) ) ;
#29342=DIRECTION ( 'NONE',  ( 0.000000000000000000, -2.173523156925980399E-06, 0.9999999999976378895 ) ) ;
#29343=CARTESIAN_POINT ( 'NONE',  ( -91.62287095715004170, -23.47596703998600631, 11.44779298504227860 ) ) ;
#29345=CARTESIAN_POINT ( 'NONE',  ( -1.843323519027639357, -20.62917239659568835, 11.49999999999998934 ) ) ;
#29347=ORIENTED_EDGE ( 'NONE', *, *, #64133, .T. ) ;
#29348=B_SPLINE_CURVE_WITH_KNOTS ( 'NONE', 3,
 ( #45479, #82524, #51589, #52085, #22109, #43481 ),
 .UNSPECIFIED., .F., .F.,
 ( 4, 2, 4 ),
 ( 0.000000000000000000, 0.001380901958385387894, 0.002761803916770775788 ),
 .UNSPECIFIED. ) ;
#29349=CARTESIAN_POINT ( 'NONE',  ( -91.52287095715010423, -24.66019654487199730, 8.947790411086115725 ) ) ;
#29353=CARTESIAN_POINT ( 'NONE',  ( 18.73254098450790295, -9.497730595714260815, -1.500000000000002220 ) ) ;
#29354=CARTESIAN_POINT ( 'NONE',  ( 18.29167757401336303, -12.14499471347784798, 11.49999999999999645 ) ) ;
#29355=CARTESIAN_POINT ( 'NONE',  ( -37.47956771133813447, -24.66019654487199730, 8.947790411086113949 ) ) ;
#29356=CARTESIAN_POINT ( 'NONE',  ( 3.584315319034878211, 22.25550262085195286, 11.49999999999998934 ) ) ;
#29357=CARTESIAN_POINT ( 'NONE',  ( -11.48448384864204996, -17.54081393385053644, -1.500000000000002220 ) ) ;
#29358=CARTESIAN_POINT ( 'NONE',  ( -89.62287095715004170, -23.47593901973091235, -1.443836447539002865 ) ) ;
#29361=ORIENTED_EDGE ( 'NONE', *, *, #90543, .T. ) ;
#29362=ORIENTED_EDGE ( 'NONE', *, *, #44216, .T. ) ;
#29365=B_SPLINE_CURVE_WITH_KNOTS ( 'NONE', 3,
 ( #1172, #71186, #94007, #93001, #32614, #31106, #23476, #32108 ),
 .UNSPECIFIED., .F., .F.,
 ( 4, 2, 2, 4 ),
 ( 6.384118678617666368E-06, 0.002007151183507260590, 0.003007534715921582075, 0.004007918248335903995 ),
 .UNSPECIFIED. ) ;
#29366=CARTESIAN_POINT ( 'NONE',  ( 7.253797376210795456, 20.28272692992397808, -1.500000000000002220 ) ) ;
#29369=VERTEX_POINT ( 'NONE', #63615 ) ;
#29370=CARTESIAN_POINT ( 'NONE',  ( -4.502559807402421121, -20.62786074129878955, 11.49999999999998934 ) ) ;
#29372=EDGE_CURVE ( 'NONE', #27253, #81452, #43656, .T. ) ;
#29374=CARTESIAN_POINT ( 'NONE',  ( -83.51346219904408485, -23.96169478059713143, 10.65365249895718058 ) ) ;
#29376=CARTESIAN_POINT ( 'NONE',  ( -70.52287095715007581, -24.99132157543166599, 2.256160258750667502 ) ) ;
#29377=CARTESIAN_POINT ( 'NONE',  ( -17.20036718215007099, 13.84871166177648583, -1.500000000000002220 ) ) ;
#29378=ADVANCED_FACE ( 'NONE', ( #87426 ), #11833, .T. ) ;
#29380=ADVANCED_FACE ( 'NONE', ( #10808 ), #95543, .T. ) ;
#29381=ORIENTED_EDGE ( 'NONE', *, *, #52998, .F. ) ;
#29382=CARTESIAN_POINT ( 'NONE',  ( -109.6485756676466252, -25.29374954521688679, 5.552272408820409844 ) ) ;
#29383=CARTESIAN_POINT ( 'NONE',  ( -79.62287095715005592, -24.64898659630528854, 1.056161002820826145 ) ) ;
#29384=CARTESIAN_POINT ( 'NONE',  ( -83.55620429048339304, -23.47593901973091235, -1.443836447539004642 ) ) ;
#29385=EDGE_CURVE ( 'NONE', #85000, #27060, #95773, .T. ) ;
#29386=DIRECTION ( 'NONE',  ( -3.773278334453080206E-23, 0.9999999999976377785, 2.173523156925979975E-06 ) ) ;
#29387=CARTESIAN_POINT ( 'NONE',  ( -5.694372300836820777, 18.57635362771370424, 11.49999999999998934 ) ) ;
#29388=CARTESIAN_POINT ( 'NONE',  ( -17.73838780825237649, 11.93509662624355450, 11.49999999999998934 ) ) ;
#29390=CARTESIAN_POINT ( 'NONE',  ( -81.55620429048339304, -23.48786465467241413, 11.44779295918255180 ) ) ;
#29391=AXIS2_PLACEMENT_3D ( 'NONE', #81081, #20167, #11557 ) ;
#29392=CARTESIAN_POINT ( 'NONE',  ( -123.5228709571500474, -23.47593901973090524, -1.443836447538996204 ) ) ;
#29394=CARTESIAN_POINT ( 'NONE',  ( 12.64511023617726160, -18.80563239904246231, -1.500000000000002220 ) ) ;
#29398=CARTESIAN_POINT ( 'NONE',  ( -3.504374479207110316, 19.46862825742285708, 11.49999999999999645 ) ) ;
#29399=CARTESIAN_POINT ( 'NONE',  ( -76.52287095715011844, -23.48783264082477373, -1.443836473390087694 ) ) ;
#29401=DIRECTION ( 'NONE',  ( -3.773278334453079618E-23, 0.9999999999976377785, 2.173523156925979975E-06 ) ) ;
#29402=CARTESIAN_POINT ( 'NONE',  ( -93.62287095715005592, -29.50248528299804818, 1.056150453629040253 ) ) ;
#29403=CARTESIAN_POINT ( 'NONE',  ( 14.58690015069645263, 15.99052346098381250, -1.500000000000002220 ) ) ;
#29404=CARTESIAN_POINT ( 'NONE',  ( -49.27110903475092130, -25.27518005823318958, 3.423268546580319871 ) ) ;
#29405=CARTESIAN_POINT ( 'NONE',  ( -2.795030477444873540, 19.22867370847827573, -1.500000000000002220 ) ) ;
#29406=CARTESIAN_POINT ( 'NONE',  ( -129.6228709571500133, -23.96177878511308634, 10.65340807706329507 ) ) ;
#29407=DIRECTION ( 'NONE',  ( -3.773278334453079618E-23, 0.9999999999976377785, 2.173523156925979975E-06 ) ) ;
#29408=CARTESIAN_POINT ( 'NONE',  ( 19.51516567812286596, -3.327523070855789911, 11.49999999999998934 ) ) ;
#29409=VECTOR ( 'NONE', #65628, 1000.000000000000114 ) ;
#29412=CARTESIAN_POINT ( 'NONE',  ( 6.737473828552405841, -19.20966278261563076, 11.49999999999999645 ) ) ;
#29416=CARTESIAN_POINT ( 'NONE',  ( -102.5093980281331483, -24.66019654487200086, 8.947790411086115725 ) ) ;
#29417=CARTESIAN_POINT ( 'NONE',  ( -27.70544111104076990, -29.50250092294406912, 8.251816161026548357 ) ) ;
#29419=CARTESIAN_POINT ( 'NONE',  ( -77.62287095715005592, -24.64965695001468404, 8.947790433994182280 ) ) ;
#29420=CARTESIAN_POINT ( 'NONE',  ( -51.36280043207702306, -25.18807129067230832, 6.689554096649111159 ) ) ;
#29421=CARTESIAN_POINT ( 'NONE',  ( -14.05898297266747221, -14.31596314050798568, -1.500000000000002220 ) ) ;
#29423=VERTEX_POINT ( 'NONE', #42288 ) ;
#29424=LINE ( 'NONE', #91327, #52780 ) ;
#29425=CARTESIAN_POINT ( 'NONE',  ( -22.75767140345847750, 1.815691853630000629, 11.49999999999999645 ) ) ;
#29426=CARTESIAN_POINT ( 'NONE',  ( -30.47287095715006799, -24.66342764659571074, 1.121861807716615145 ) ) ;
#29427=CARTESIAN_POINT ( 'NONE',  ( -96.52287095715006160, -29.50250243563736774, 8.947779886222138046 ) ) ;
#29429=CARTESIAN_POINT ( 'NONE',  ( -89.62287095715004170, -23.47593901973091235, -1.443836447539002865 ) ) ;
#29430=EDGE_CURVE ( 'NONE', #62504, #18736, #84789, .T. ) ;
#29432=CARTESIAN_POINT ( 'NONE',  ( -117.5895376238167245, -23.47596703998600631, 11.44779298504227683 ) ) ;
#29437=CARTESIAN_POINT ( 'NONE',  ( -17.59887021274124663, -10.25344800880639262, 11.49999999999998934 ) ) ;
#29438=EDGE_LOOP ( 'NONE', ( #88141, #99458, #97049, #49400 ) ) ;
#29439=CARTESIAN_POINT ( 'NONE',  ( 22.74528686061176685, 3.085755641335488964, -1.500000000000002220 ) ) ;
#29440=DIRECTION ( 'NONE',  ( -3.773278334453079618E-23, 0.9999999999976377785, 2.173523156925979975E-06 ) ) ;
#29441=ORIENTED_EDGE ( 'NONE', *, *, #78387, .F. ) ;
#29442=DIRECTION ( 'NONE',  ( 3.773278334444166432E-23, -1.000000000000000000, 0.000000000000000000 ) ) ;
#29443=CARTESIAN_POINT ( 'NONE',  ( -77.50430339230356935, -24.35071581493544102, 9.817618358456021710 ) ) ;
#29444=CARTESIAN_POINT ( 'NONE',  ( -80.96226385320382235, -25.13069340115295702, 2.947789388436138580 ) ) ;
#29445=CARTESIAN_POINT ( 'NONE',  ( 21.11169859150035677, 2.410084449224629832, 11.49999999999999645 ) ) ;
#29446=ORIENTED_EDGE ( 'NONE', *, *, #56732, .F. ) ;
#29447=ORIENTED_EDGE ( 'NONE', *, *, #85284, .T. ) ;
#29448=CARTESIAN_POINT ( 'NONE',  ( -7.477829544921322125, 20.88912457518834742, 11.49999999999998934 ) ) ;
#29450=CARTESIAN_POINT ( 'NONE',  ( -15.40095275084150117, -13.70674696055758801, 11.49999999999998934 ) ) ;
#29451=B_SPLINE_CURVE_WITH_KNOTS ( 'NONE', 3,
 ( #41136, #1064, #56371, #49259, #87291, #8675 ),
 .UNSPECIFIED., .F., .F.,
 ( 4, 2, 4 ),
 ( 6.384118678621234070E-06, 0.001386860460828383441, 0.002767336802978145362 ),
 .UNSPECIFIED. ) ;
#29452=VERTEX_POINT ( 'NONE', #51371 ) ;
#29454=DIRECTION ( 'NONE',  ( 0.000000000000000000, 0.9999999999976377785, 2.173523156925979975E-06 ) ) ;
#29455=CARTESIAN_POINT ( 'NONE',  ( -54.62287095715004170, -23.47596703998600631, 11.44779298504227505 ) ) ;
#29457=ORIENTED_EDGE ( 'NONE', *, *, #31082, .F. ) ;
#29459=CARTESIAN_POINT ( 'NONE',  ( -111.6286693378537507, -23.96169478059714564, 10.65365249895717348 ) ) ;
#29460=CARTESIAN_POINT ( 'NONE',  ( -48.52287095715007581, -23.72747288104470087, -1.053458166803227458 ) ) ;
#29461=CARTESIAN_POINT ( 'NONE',  ( 11.56195852851363526, -17.29799701895051811, -1.500000000000002220 ) ) ;
#29462=CARTESIAN_POINT ( 'NONE',  ( 4.771108217193557266, 21.26182814020628697, 11.49999999999999645 ) ) ;
#29463=CARTESIAN_POINT ( 'NONE',  ( -39.66923462213467388, -25.22668475970086988, 3.617326360174414113 ) ) ;
#29465=CARTESIAN_POINT ( 'NONE',  ( -0.1411031551986380028, 22.44022050402121948, 11.49999999999998934 ) ) ;
#29466=CARTESIAN_POINT ( 'NONE',  ( -51.28074245548943111, -25.26334620367392247, 4.131999547932733385 ) ) ;
#29467=EDGE_CURVE ( 'NONE', #74882, #18460, #81217, .T. ) ;
#29468=VERTEX_POINT ( 'NONE', #66621 ) ;
#29469=CARTESIAN_POINT ( 'NONE',  ( -75.52287095715013265, -24.91544648472621049, 1.928969306349232582 ) ) ;
#29471=CARTESIAN_POINT ( 'NONE',  ( -69.52287095715010423, -24.33927499327855770, 9.819080762295813614 ) ) ;
#29474=ORIENTED_EDGE ( 'NONE', *, *, #32480, .T. ) ;
#29477=CARTESIAN_POINT ( 'NONE',  ( -18.64022381217131397, 10.26305532446727753, -1.500000000000002220 ) ) ;
#29480=CARTESIAN_POINT ( 'NONE',  ( -20.98013922110768448, -1.350454208470041273, 11.49999999999998934 ) ) ;
#29481=CARTESIAN_POINT ( 'NONE',  ( -125.5228709571500616, -23.48783264083375144, -1.443836473376139740 ) ) ;
#29482=EDGE_CURVE ( 'NONE', #59175, #86526, #75086, .T. ) ;
#29484=PLANE ( 'NONE',  #12584 ) ;
#29485=CARTESIAN_POINT ( 'NONE',  ( 1.548332177993611225, -21.85883989728069565, -1.500000000000002220 ) ) ;
#29486=CARTESIAN_POINT ( 'NONE',  ( -87.54287996507414960, -24.65952944569304606, 1.056160979905703678 ) ) ;
#29491=B_SPLINE_CURVE_WITH_KNOTS ( 'NONE', 3,
 ( #78195, #62494, #16306, #15803, #63008, #54886 ),
 .UNSPECIFIED., .F., .F.,
 ( 4, 2, 4 ),
 ( 0.000000000000000000, 0.001380764517853245565, 0.002761529035706491129 ),
 .UNSPECIFIED. ) ;
#29492=CARTESIAN_POINT ( 'NONE',  ( -84.50113732502067876, -24.66019654487200441, 8.947790411086115725 ) ) ;
#29494=CARTESIAN_POINT ( 'NONE',  ( -130.5728709571500588, -24.66513809378597344, 8.909134979017292011 ) ) ;
#29495=CARTESIAN_POINT ( 'NONE',  ( -39.52287095715006870, -29.50248528299804818, 1.056150453629031594 ) ) ;
#29496=CARTESIAN_POINT ( 'NONE',  ( 20.93798385506118365, 3.901641247904229282, -1.500000000000002220 ) ) ;
#29497=CARTESIAN_POINT ( 'NONE',  ( -112.5222218763195912, -23.48783264082478794, -1.443836473390061270 ) ) ;
#29498=EDGE_CURVE ( 'NONE', #12184, #53220, #1234, .T. ) ;
#29499=CARTESIAN_POINT ( 'NONE',  ( -107.5572310827927396, -23.73791477778912551, 11.05961554403170055 ) ) ;
#29500=CARTESIAN_POINT ( 'NONE',  ( -60.92287095715005307, -23.47596703998600631, 11.44779298504227683 ) ) ;
#29502=CARTESIAN_POINT ( 'NONE',  ( 14.18375884139645215, 17.39688726336347102, -1.500000000000002220 ) ) ;
#29504=B_SPLINE_SURFACE_WITH_KNOTS ( 'NONE', 3, 3, ( 
 ( #63943, #87751, #78109, #18235 ),
 ( #64940, #57323, #16227, #70521 ),
 ( #1011, #55310, #35957, #65936 ),
 ( #49705, #82131, #57815, #19227 ),
 ( #13106, #80635, #5007, #4520 ),
 ( #66926, #88757, #50192, #73526 ),
 ( #96359, #98341, #51690, #11119 ) ),
 .UNSPECIFIED., .F., .F., .F.,
 ( 4, 3, 4 ),
 ( 4, 4 ),
 ( 0.7945040050992245861, 0.8970133687736505657, 0.9995227324480766562 ),
 ( 0.7696895860335216666, 0.7710576503773675094 ),
 .UNSPECIFIED. ) ;
#29506=ORIENTED_EDGE ( 'NONE', *, *, #75083, .F. ) ;
#29507=CARTESIAN_POINT ( 'NONE',  ( -72.62287095715005592, -23.48783264082478084, -1.443836473390067265 ) ) ;
#29508=CARTESIAN_POINT ( 'NONE',  ( -19.57149217635686966, 1.386223266712492297, 11.49999999999999645 ) ) ;
#29509=CARTESIAN_POINT ( 'NONE',  ( -42.62287095715004881, -23.47593901973091235, -1.443836447539011525 ) ) ;
#29510=CARTESIAN_POINT ( 'NONE',  ( -119.5562042904833930, -23.47593901973091235, -1.443836447538997536 ) ) ;
#29511=EDGE_CURVE ( 'NONE', #79117, #83628, #52100, .T. ) ;
#29513=CARTESIAN_POINT ( 'NONE',  ( -88.55825211740739178, -23.73791477778912196, 11.05961554403170588 ) ) ;
#29514=CARTESIAN_POINT ( 'NONE',  ( -108.5228709571501042, -24.66019654487200441, 8.947790411086113949 ) ) ;
#29515=CARTESIAN_POINT ( 'NONE',  ( -90.93551152535891902, -25.12049752546737480, 2.832404795212227100 ) ) ;
#29516=CARTESIAN_POINT ( 'NONE',  ( -26.73206948527849747, -24.64631784552947380, 7.985388846607621716 ) ) ;
#29517=CARTESIAN_POINT ( 'NONE',  ( -14.27994306655487300, -13.59162091658854798, -1.500000000000002220 ) ) ;
#29518=EDGE_LOOP ( 'NONE', ( #30417, #70643, #4524, #17903 ) ) ;
#29521=LINE ( 'NONE', #60500, #31054 ) ;
#29526=CARTESIAN_POINT ( 'NONE',  ( -45.62287095715005592, -23.48786465467240703, 11.44779295918255002 ) ) ;
#29527=CARTESIAN_POINT ( 'NONE',  ( -55.59975228423683546, -24.15503026093915295, -0.2815557561904505901 ) ) ;
#29528=CARTESIAN_POINT ( 'NONE',  ( -50.62287095715005592, -24.99156045073392463, 7.747789690856161648 ) ) ;
#29529=CARTESIAN_POINT ( 'NONE',  ( -49.52287095715006160, -24.64965694238406613, 8.947790433994203596 ) ) ;
#29530=B_SPLINE_CURVE_WITH_KNOTS ( 'NONE', 3,
 ( #85055, #17047, #2848, #3844 ),
 .UNSPECIFIED., .F., .F.,
 ( 4, 4 ),
 ( 0.4508219208986671278, 0.4598283521707824950 ),
 .UNSPECIFIED. ) ;
#29533=CARTESIAN_POINT ( 'NONE',  ( -0.003041637939312698616, 19.98351707251910980, 11.49999999999998934 ) ) ;
#29534=ADVANCED_FACE ( 'NONE', ( #97535 ), #5400, .T. ) ;
#29535=B_SPLINE_CURVE_WITH_KNOTS ( 'NONE', 3,
 ( #29509, #4694, #27533, #74203 ),
 .UNSPECIFIED., .F., .F.,
 ( 4, 4 ),
 ( 0.1198715217971635938, 0.1288779530692791553 ),
 .UNSPECIFIED. ) ;
#29536=CARTESIAN_POINT ( 'NONE',  ( -123.5228709571501184, -24.66019654487200441, 8.947790411086105067 ) ) ;
#29537=CARTESIAN_POINT ( 'NONE',  ( -51.69697151907276123, -25.28137579932158729, 4.089352667124304119 ) ) ;
#29538=VERTEX_POINT ( 'NONE', #38632 ) ;
#29540=ADVANCED_FACE ( 'NONE', ( #54373, #75 ), #80692, .T. ) ;
#29544=CARTESIAN_POINT ( 'NONE',  ( -80.49583835628830286, -24.83644354573579349, 8.397322867130094792 ) ) ;
#29545=CARTESIAN_POINT ( 'NONE',  ( -81.55620429048337883, -23.48783264082478084, -1.443836473390065933 ) ) ;
#29546=CARTESIAN_POINT ( 'NONE',  ( -114.5228709571500616, -29.50250243563736774, 8.947779886222136270 ) ) ;
#29551=ADVANCED_FACE ( 'NONE', ( #21889 ), #36180, .T. ) ;
#29553=VERTEX_POINT ( 'NONE', #78185 ) ;
#29554=CARTESIAN_POINT ( 'NONE',  ( -13.42616926349082895, -15.17935092467416069, -1.500000000000002220 ) ) ;
#29555=VECTOR ( 'NONE', #61570, 1000.000000000000114 ) ;
#29556=CARTESIAN_POINT ( 'NONE',  ( -122.6271156531370394, -23.48783264082477373, -1.443836473390087471 ) ) ;
#29557=PLANE ( 'NONE',  #7970 ) ;
#29559=VERTEX_POINT ( 'NONE', #94926 ) ;
#29561=CARTESIAN_POINT ( 'NONE',  ( -63.62287095715002749, -23.94994826722514958, -0.6494450866351725304 ) ) ;
#29562=CARTESIAN_POINT ( 'NONE',  ( 9.271505649751263789, 17.87650053469100087, -1.500000000000002220 ) ) ;
#29563=CARTESIAN_POINT ( 'NONE',  ( -5.931750313267273533, -20.21149935180699231, 11.49999999999999645 ) ) ;
#29564=B_SPLINE_CURVE_WITH_KNOTS ( 'NONE', 3,
 ( #10493, #49575, #41453, #33834 ),
 .UNSPECIFIED., .F., .F.,
 ( 4, 4 ),
 ( 0.4100787516764388130, 0.4190851829485544022 ),
 .UNSPECIFIED. ) ;
#29565=SHELL_BASED_SURFACE_MODEL ( 'NONE', ( #77601, #64681 ) );
#29567=CARTESIAN_POINT ( 'NONE',  ( -19.11006845027251799, 11.06304553819242642, -1.500000000000002220 ) ) ;
#29569=CARTESIAN_POINT ( 'NONE',  ( -1.764913036440812322, 20.45846032914734280, 11.49999999999998934 ) ) ;
#29572=CARTESIAN_POINT ( 'NONE',  ( -59.52287095715006160, -24.64898659630528854, 1.056161002820822592 ) ) ;
#29574=CARTESIAN_POINT ( 'NONE',  ( -123.6228709571500559, -29.50250243563736774, 8.947779886222134493 ) ) ;
#29575=EDGE_LOOP ( 'NONE', ( #84246, #87085, #72816, #19842 ) ) ;
#29576=CARTESIAN_POINT ( 'NONE',  ( -83.52287095715006160, -23.47596703998600631, 11.44779298504228571 ) ) ;
#29577=CARTESIAN_POINT ( 'NONE',  ( -64.58953762381672448, -24.64965694238407323, 8.947790433994656567 ) ) ;
#29578=ORIENTED_EDGE ( 'NONE', *, *, #4094, .T. ) ;
#29580=CARTESIAN_POINT ( 'NONE',  ( -118.6228709571500701, -23.94994826722515668, -0.6494450866351694218 ) ) ;
#29582=CARTESIAN_POINT ( 'NONE',  ( -76.52212344122790455, -23.48783264082477373, -1.443836473390089026 ) ) ;
#29583=CARTESIAN_POINT ( 'NONE',  ( 11.79242832063081892, -16.95861370568002613, -1.500000000000002220 ) ) ;
#29584=CARTESIAN_POINT ( 'NONE',  ( 5.819084965910729323, 20.79142713412266730, 11.49999999999999645 ) ) ;
#29587=CARTESIAN_POINT ( 'NONE',  ( -56.62287095715005592, -23.47593901973091235, -1.443836447539007972 ) ) ;
#29588=CARTESIAN_POINT ( 'NONE',  ( 13.91197278145025074, 17.48688927191260234, -1.500000000000002220 ) ) ;
#29589=CARTESIAN_POINT ( 'NONE',  ( -48.58953762381672448, -23.48786465467241058, 11.44779295918254824 ) ) ;
#29592=CARTESIAN_POINT ( 'NONE',  ( -104.6228709571500559, -29.50250786944525672, 11.44777988621623166 ) ) ;
#29593=CARTESIAN_POINT ( 'NONE',  ( -49.62827599070762830, -24.51419770103158413, 9.386484678747189392 ) ) ;
#29595=CARTESIAN_POINT ( 'NONE',  ( 20.89859092893058801, 0.06103081833375877813, 11.49999999999998934 ) ) ;
#29597=CARTESIAN_POINT ( 'NONE',  ( -67.62720759924459912, -24.51419770103159124, 9.386484678747168076 ) ) ;
#29599=ORIENTED_EDGE ( 'NONE', *, *, #77885, .F. ) ;
#29600=CARTESIAN_POINT ( 'NONE',  ( -109.5138029155384203, -24.51419770103157347, 9.386484678747171628 ) ) ;
#29601=CARTESIAN_POINT ( 'NONE',  ( -0.2625952501129409367, 21.13516572482953748, -1.500000000000002220 ) ) ;
#29603=CARTESIAN_POINT ( 'NONE',  ( -123.2228709571500502, -23.47596703998600631, 11.44779298504227860 ) ) ;
#29604=CARTESIAN_POINT ( 'NONE',  ( -99.69221343823950576, -25.26221271103905153, 6.884718109595215019 ) ) ;
#29605=CARTESIAN_POINT ( 'NONE',  ( 21.63681353182189682, 2.665401433100548889, -1.500000000000002220 ) ) ;
#29606=DIRECTION ( 'NONE',  ( -0.000000000000000000, 2.173523156925979552E-06, -0.9999999999976378895 ) ) ;
#29607=CARTESIAN_POINT ( 'NONE',  ( -86.52287095715006160, -29.50250786944525672, 11.44777988621623344 ) ) ;
#29609=CARTESIAN_POINT ( 'NONE',  ( 14.84582651547613352, 15.88809324551894520, -1.500000000000002220 ) ) ;
#29610=CARTESIAN_POINT ( 'NONE',  ( -79.53598664403750718, -25.10472966370973325, 7.258571028815275383 ) ) ;
#29612=CARTESIAN_POINT ( 'NONE',  ( -21.16112330106665240, 7.131417522999676351, 11.49999999999999645 ) ) ;
#29613=VERTEX_POINT ( 'NONE', #95429 ) ;
#29614=CARTESIAN_POINT ( 'NONE',  ( -116.5562042904834215, -23.47593901973091235, -1.443836447538997536 ) ) ;
#29618=ORIENTED_EDGE ( 'NONE', *, *, #63106, .F. ) ;
#29622=CARTESIAN_POINT ( 'NONE',  ( 15.88337727998148985, 12.78846505907953279, -1.500000000000002220 ) ) ;
#29623=EDGE_CURVE ( 'NONE', #73093, #58493, #60546, .T. ) ;
#29624=CARTESIAN_POINT ( 'NONE',  ( -120.6228709571500417, -24.99156045073393528, 7.747789690856161648 ) ) ;
#29625=CARTESIAN_POINT ( 'NONE',  ( 15.88363568188429653, -14.04911357082368006, 11.49999999999998934 ) ) ;
#29628=CARTESIAN_POINT ( 'NONE',  ( -80.40044610398997804, -25.27791972731367309, 7.562158963542455758 ) ) ;
#29629=CARTESIAN_POINT ( 'NONE',  ( -99.58953762381672448, -24.64898659630367916, 1.056161002820388717 ) ) ;
#29632=CARTESIAN_POINT ( 'NONE',  ( -37.62287095715007013, -24.51387760970723662, 9.387446482453421837 ) ) ;
#29633=CARTESIAN_POINT ( 'NONE',  ( -38.52287095715006870, -23.47593901973090169, -1.443836447538997092 ) ) ;
#29634=ORIENTED_EDGE ( 'NONE', *, *, #4149, .F. ) ;
#29635=CARTESIAN_POINT ( 'NONE',  ( 16.20606029192996900, -10.75321813762353251, 11.49999999999999645 ) ) ;
#29636=CARTESIAN_POINT ( 'NONE',  ( -60.52287095715006160, -24.99132157543083821, 2.256160258750667502 ) ) ;
#29637=AXIS2_PLACEMENT_3D ( 'NONE', #19117, #27246, #35362 ) ;
#29642=DIRECTION ( 'NONE',  ( -0.6837407958605439262, 0.000000000000000000, 0.7297249646791521549 ) ) ;
#29643=DIRECTION ( 'NONE',  ( -0.000000000000000000, 0.5420701495772373146, 0.8403332392196035672 ) ) ;
#29644=CARTESIAN_POINT ( 'NONE',  ( -15.21066300689680872, 12.40131300380995860, -1.500000000000002220 ) ) ;
#29645=B_SPLINE_SURFACE_WITH_KNOTS ( 'NONE', 3, 3, ( 
 ( #88806, #73083, #65988, #66490 ),
 ( #26399, #49754, #19271, #81685 ),
 ( #3074, #88301, #4064, #50243 ),
 ( #87798, #18772, #3569, #17787 ),
 ( #56867, #12158, #34013, #42640 ),
 ( #72580, #2568, #41132, #64989 ),
 ( #18284, #48750, #11171, #79673 ) ),
 .UNSPECIFIED., .F., .F., .F.,
 ( 4, 3, 4 ),
 ( 4, 4 ),
 ( 0.2469299128580444980, 0.4952425859456087709, 0.7435552590331729883 ),
 ( 0.02428983952429602036, 0.1659897170784108700 ),
 .UNSPECIFIED. ) ;
#29646=DIRECTION ( 'NONE',  ( 0.000000000000000000, -2.173523156925980399E-06, 0.9999999999976378895 ) ) ;
#29648=CARTESIAN_POINT ( 'NONE',  ( 20.54099941694853726, 6.510794959084822864, 11.49999999999998934 ) ) ;
#29649=CARTESIAN_POINT ( 'NONE',  ( -33.49675094381932894, -24.15620529776627379, 10.23563542870661536 ) ) ;
#29650=CARTESIAN_POINT ( 'NONE',  ( -96.52287095715010423, -23.48783264082477018, -1.443836473390086139 ) ) ;
#29652=CARTESIAN_POINT ( 'NONE',  ( -99.84936175820153892, -25.27473256197501783, 3.453118245436027856 ) ) ;
#29653=CARTESIAN_POINT ( 'NONE',  ( -8.820007276677138464, 21.28423624206370945, -1.500000000000002220 ) ) ;
#29655=CARTESIAN_POINT ( 'NONE',  ( -93.55476215406292795, -23.96119346886881019, -0.6495511937832080251 ) ) ;
#29656=CARTESIAN_POINT ( 'NONE',  ( -129.5228709571500758, -29.50250243563736774, 8.947779886222132717 ) ) ;
#29657=CARTESIAN_POINT ( 'NONE',  ( 20.05498121024909253, 1.910150955369836812, 11.49999999999999645 ) ) ;
#29659=CARTESIAN_POINT ( 'NONE',  ( -91.52287095715013265, -23.96127896941632685, -0.6493128931038013585 ) ) ;
#29660=CARTESIAN_POINT ( 'NONE',  ( -82.62287095715005592, -29.50250243563736774, 8.947779886222141599 ) ) ;
#29662=CARTESIAN_POINT ( 'NONE',  ( -110.3346797185884327, -25.29779155363456056, 3.293942871399098138 ) ) ;
#29663=EDGE_CURVE ( 'NONE', #83541, #39939, #57393, .T. ) ;
#29664=CARTESIAN_POINT ( 'NONE',  ( 0.1862606309321278575, -19.90735222434816976, 11.49999999999998934 ) ) ;
#29666=CARTESIAN_POINT ( 'NONE',  ( -97.52287095715006160, -23.48786465467241769, 11.44779295918254114 ) ) ;
#29667=CARTESIAN_POINT ( 'NONE',  ( 19.60560811685724403, 2.727087469661350738, -1.500000000000002220 ) ) ;
#29668=CARTESIAN_POINT ( 'NONE',  ( -126.6242556467910845, -24.15620529776629510, 10.23563542870658871 ) ) ;
#29669=EDGE_CURVE ( 'NONE', #58438, #4006, #83529, .T. ) ;
#29672=CARTESIAN_POINT ( 'NONE',  ( -110.5228709571500616, -23.84081130425355610, 10.88220057483161440 ) ) ;
#29674=CARTESIAN_POINT ( 'NONE',  ( -20.26430336558559020, 4.098603726722801710, 11.49999999999999645 ) ) ;
#29675=CARTESIAN_POINT ( 'NONE',  ( -98.52287095715006160, -24.64898659630368272, 1.056161002820829697 ) ) ;
#29676=EDGE_CURVE ( 'NONE', #44716, #12095, #8696, .T. ) ;
#29678=CARTESIAN_POINT ( 'NONE',  ( -49.59985430115347071, -25.25138735060574646, 5.484775612577745818 ) ) ;
#29679=CARTESIAN_POINT ( 'NONE',  ( 4.564784964189898098, -22.25151590922551748, 11.49999999999999645 ) ) ;
#29680=ADVANCED_FACE ( 'NONE', ( #55377 ), #32527, .F. ) ;
#29682=CARTESIAN_POINT ( 'NONE',  ( -78.62287095715004170, -24.65952944569304606, 1.056160979905698349 ) ) ;
#29684=CARTESIAN_POINT ( 'NONE',  ( -15.75104486599040321, 12.61009050114280861, 11.49999999999998934 ) ) ;
#29685=CARTESIAN_POINT ( 'NONE',  ( -63.55959536319858927, -23.73766607897669445, -1.055555164236456900 ) ) ;
#29687=ORIENTED_EDGE ( 'NONE', *, *, #54019, .F. ) ;
#29688=ORIENTED_EDGE ( 'NONE', *, *, #45875, .F. ) ;
#29691=CARTESIAN_POINT ( 'NONE',  ( 22.85676281555306844, 1.471244944367766649, -1.500000000000002220 ) ) ;
#29692=PLANE ( 'NONE',  #24346 ) ;
#29693=CARTESIAN_POINT ( 'NONE',  ( -10.14273968512601520, 19.10955606681249463, -1.500000000000002220 ) ) ;
#29694=LINE ( 'NONE', #75359, #17190 ) ;
#29695=CARTESIAN_POINT ( 'NONE',  ( -112.6228709571500559, -23.47596703998600631, 11.44779298504227860 ) ) ;
#29696=CARTESIAN_POINT ( 'NONE',  ( -8.531171415479239073, -19.09552649099111221, 11.49999999999999645 ) ) ;
#29698=CARTESIAN_POINT ( 'NONE',  ( -28.04192716165177401, -24.82017564189413861, 2.322794568040253083 ) ) ;
#29699=CARTESIAN_POINT ( 'NONE',  ( 0.3405503412851532130, 21.98688381012616233, -1.500000000000002220 ) ) ;
#29701=CARTESIAN_POINT ( 'NONE',  ( -105.5874363681110140, -24.73531770709095312, 8.716586749053508498 ) ) ;
#29702=CARTESIAN_POINT ( 'NONE',  ( -27.68651082257923335, -25.21724994476180015, 7.605671628963411202 ) ) ;
#29703=VECTOR ( 'NONE', #48907, 1000.000000000000114 ) ;
#29705=FACE_OUTER_BOUND ( 'NONE', #98713, .T. ) ;
#29706=CARTESIAN_POINT ( 'NONE',  ( -90.50111960292845481, -24.83644354573578994, 8.397322867130100121 ) ) ;
#29707=ORIENTED_EDGE ( 'NONE', *, *, #32939, .T. ) ;
#29712=ORIENTED_EDGE ( 'NONE', *, *, #71467, .T. ) ;
#29713=CARTESIAN_POINT ( 'NONE',  ( -71.63517953107638903, -24.15620529776628445, 10.23563542870660115 ) ) ;
#29714=CARTESIAN_POINT ( 'NONE',  ( -101.6521089408578007, -25.27404798564288058, 3.606142184538064566 ) ) ;
#29715=CARTESIAN_POINT ( 'NONE',  ( -104.5599248761161562, -23.48786465467241413, 11.44779295918254469 ) ) ;
#29716=CARTESIAN_POINT ( 'NONE',  ( 20.39576089869593289, -0.2533167397448486957, -1.500000000000002220 ) ) ;
#29721=ADVANCED_FACE ( 'NONE', ( #5571 ), #96916, .T. ) ;
#29723=CARTESIAN_POINT ( 'NONE',  ( -91.52287095715004739, -24.50216790748205042, 0.6166512839542547253 ) ) ;
#29726=CARTESIAN_POINT ( 'NONE',  ( -29.74590468580106872, -25.26247595756167286, 6.038516002892558632 ) ) ;
#29727=CARTESIAN_POINT ( 'NONE',  ( 6.705275102110877405, 19.67741782454948662, -1.500000000000002220 ) ) ;
#29728=ORIENTED_EDGE ( 'NONE', *, *, #96526, .F. ) ;
#29729=CARTESIAN_POINT ( 'NONE',  ( -54.62287095715005592, -23.47593901973091235, -1.443836447539009749 ) ) ;
#29730=ORIENTED_EDGE ( 'NONE', *, *, #2474, .F. ) ;
#29731=B_SPLINE_SURFACE_WITH_KNOTS ( 'NONE', 3, 3, ( 
 ( #78423, #77416, #23128, #54117 ),
 ( #7920, #62226, #23631, #54605 ),
 ( #811, #8920, #78922, #85540 ),
 ( #70830, #32258, #63228, #55616 ),
 ( #16024, #94150, #86544, #17031 ),
 ( #47997, #9415, #26656, #87551 ),
 ( #89056, #42887, #49503, #40875 ) ),
 .UNSPECIFIED., .F., .F., .F.,
 ( 4, 3, 4 ),
 ( 4, 4 ),
 ( 0.7945040050992246972, 0.8970133687736503436, 0.9995227324480758790 ),
 ( 0.3595853728713703235, 0.3607641058962429148 ),
 .UNSPECIFIED. ) ;
#29732=CARTESIAN_POINT ( 'NONE',  ( -68.52287095715011844, -24.33927499327855060, 9.819080762295813614 ) ) ;
#29734=ORIENTED_EDGE ( 'NONE', *, *, #23637, .T. ) ;
#29736=CARTESIAN_POINT ( 'NONE',  ( -92.62287095715005592, -24.66019654487199730, 8.947790411086124607 ) ) ;
#29737=B_SPLINE_CURVE_WITH_KNOTS ( 'NONE', 3,
 ( #30909, #46651, #60875, #69478 ),
 .UNSPECIFIED., .F., .F.,
 ( 4, 4 ),
 ( 0.000000000000000000, 9.999999999998897304E-05 ),
 .UNSPECIFIED. ) ;
#29738=CARTESIAN_POINT ( 'NONE',  ( -64.52287095715007581, -23.96177878511308279, 10.65340807706329684 ) ) ;
#29739=CARTESIAN_POINT ( 'NONE',  ( -100.4498239493576506, -25.25419554228399832, 7.563173735396891750 ) ) ;
#29740=DIRECTION ( 'NONE',  ( 3.773278334444167608E-23, -1.000000000000000000, 0.000000000000000000 ) ) ;
#29743=CARTESIAN_POINT ( 'NONE',  ( -11.88820881604258339, -18.65297325734525913, 11.49999999999999645 ) ) ;
#29745=CARTESIAN_POINT ( 'NONE',  ( -44.62287095715004881, -24.66019654487198665, 8.947790411086135265 ) ) ;
#29746=VECTOR ( 'NONE', #18888, 1000.000000000000114 ) ;
#29747=CARTESIAN_POINT ( 'NONE',  ( 22.64978874513612439, 0.4204215919581203442, -1.500000000000002220 ) ) ;
#29749=ORIENTED_EDGE ( 'NONE', *, *, #1248, .F. ) ;
#29754=CARTESIAN_POINT ( 'NONE',  ( -11.28321777122536140, 16.66956161807075887, -1.500000000000002220 ) ) ;
#29755=EDGE_CURVE ( 'NONE', #55213, #89773, #51255, .T. ) ;
#29756=CARTESIAN_POINT ( 'NONE',  ( -19.06493965993949402, -22.58124009362228435, -1.443836447538997536 ) ) ;
#29757=VERTEX_POINT ( 'NONE', #19787 ) ;
#29759=CARTESIAN_POINT ( 'NONE',  ( -0.4079105510268487000, 22.33655531192813370, -1.500000000000002220 ) ) ;
#29760=EDGE_CURVE ( 'NONE', #95000, #7634, #53358, .T. ) ;
#29762=VERTEX_POINT ( 'NONE', #12177 ) ;
#29764=CARTESIAN_POINT ( 'NONE',  ( -81.67164698139400514, -25.15124539077181609, 6.939751081170221880 ) ) ;
#29765=CARTESIAN_POINT ( 'NONE',  ( -49.74369414166532977, -29.50249372652338664, 4.940868828539293212 ) ) ;
#29768=CARTESIAN_POINT ( 'NONE',  ( -80.55620429048337883, -24.99156044556201905, 7.747789690856173195 ) ) ;
#29769=CARTESIAN_POINT ( 'NONE',  ( 11.58774116221665729, 15.72987433093905096, -1.500000000000002220 ) ) ;
#29770=CARTESIAN_POINT ( 'NONE',  ( -47.52287095715003318, -23.73907113217730469, -1.053371485780176142 ) ) ;
#29771=CARTESIAN_POINT ( 'NONE',  ( -16.68621059303058018, 13.52761613308161870, -1.500000000000002220 ) ) ;
#29772=CARTESIAN_POINT ( 'NONE',  ( -25.64067666839992299, -24.92775104721833657, 3.645611680657319109 ) ) ;
#29774=CARTESIAN_POINT ( 'NONE',  ( -34.52287095715008292, -23.94994826722564696, -0.6494450866342749151 ) ) ;
#29775=CARTESIAN_POINT ( 'NONE',  ( -22.64140897529919272, -3.284158816904186651, -1.500000000000002220 ) ) ;
#29777=PLANE ( 'NONE',  #38543 ) ;
#29779=CARTESIAN_POINT ( 'NONE',  ( 16.76344175524385705, -10.90933549886441156, 11.49999999999999645 ) ) ;
#29780=CARTESIAN_POINT ( 'NONE',  ( -50.52287095715008292, -23.85196035786900026, -0.8779234886475190125 ) ) ;
#29781=VECTOR ( 'NONE', #67238, 1000.000000000000114 ) ;
#29782=CARTESIAN_POINT ( 'NONE',  ( -74.55412444941374872, -23.96169478059713498, 10.65365249895717881 ) ) ;
#29783=CARTESIAN_POINT ( 'NONE',  ( -37.62287095715005592, -24.64898659630367206, 1.056161002820819261 ) ) ;
#29784=ORIENTED_EDGE ( 'NONE', *, *, #47369, .T. ) ;
#29785=CARTESIAN_POINT ( 'NONE',  ( -26.57207785542718170, -24.62921250442780874, 2.000914044556121762 ) ) ;
#29786=CARTESIAN_POINT ( 'NONE',  ( -65.52287095715007581, -24.52323809116984066, 9.355190652339423707 ) ) ;
#29787=CARTESIAN_POINT ( 'NONE',  ( -20.31635052000798325, -7.690577546848336610, -1.500000000000002220 ) ) ;
#29788=CARTESIAN_POINT ( 'NONE',  ( -77.58953762381672448, -24.66019654487199730, 8.947790411086112172 ) ) ;
#29789=CARTESIAN_POINT ( 'NONE',  ( 15.22544387773384500, -12.34335808662847178, -1.500000000000002220 ) ) ;
#29790=CARTESIAN_POINT ( 'NONE',  ( -100.0958943179937961, -25.13913306373530077, 7.067219463468185303 ) ) ;
#29791=ADVANCED_FACE ( 'NONE', ( #96928 ), #5071, .F. ) ;
#29794=DIRECTION ( 'NONE',  ( -0.04174795870516300605, 0.5404601326709027598, 0.8403332392195981271 ) ) ;
#29795=CARTESIAN_POINT ( 'NONE',  ( -47.52287095715006160, -23.47596703998600631, 11.44779298504229104 ) ) ;
#29796=CARTESIAN_POINT ( 'NONE',  ( -20.35906544237474236, -2.577633573104691322, 11.49999999999999645 ) ) ;
#29801=CARTESIAN_POINT ( 'NONE',  ( -39.89668141102733756, -25.28892453938336615, 3.440461006402131705 ) ) ;
#29802=CARTESIAN_POINT ( 'NONE',  ( -101.5228709571500900, -23.48783264082477018, -1.443836473390087249 ) ) ;
#29804=AXIS2_PLACEMENT_3D ( 'NONE', #86354, #70627, #16837 ) ;
#29806=CARTESIAN_POINT ( 'NONE',  ( -5.338719972479099241, 22.46511350730333589, 11.49999999999999645 ) ) ;
#29807=CARTESIAN_POINT ( 'NONE',  ( 22.80427751693360960, 0.003464389817739472934, 11.49999999999998934 ) ) ;
#29808=CARTESIAN_POINT ( 'NONE',  ( -110.5598947927333739, -23.48786465467241413, 11.44779295918253581 ) ) ;
#29812=CARTESIAN_POINT ( 'NONE',  ( -115.5228709571500616, -25.00158670708909625, 2.256160236439166411 ) ) ;
#29813=CARTESIAN_POINT ( 'NONE',  ( -110.5493975497841461, -24.83618233451450763, 1.606449574219537935 ) ) ;
#29814=CARTESIAN_POINT ( 'NONE',  ( -14.06357901826416068, -16.81340526219955933, 11.49999999999998934 ) ) ;
#29818=CARTESIAN_POINT ( 'NONE',  ( -87.50769031727142533, -24.35071581493543391, 9.817618358456025263 ) ) ;
#29819=CARTESIAN_POINT ( 'NONE',  ( -34.62287095715005592, -24.66019654487199020, 8.947790411086137041 ) ) ;
#29820=CARTESIAN_POINT ( 'NONE',  ( -78.59205981310179823, -24.15543982623907127, -0.2315651400026641771 ) ) ;
#29821=CARTESIAN_POINT ( 'NONE',  ( -79.62287095715005592, -23.48786465467241058, 11.44779295918254469 ) ) ;
#29822=CARTESIAN_POINT ( 'NONE',  ( -73.62287095715005592, -23.48786465467241058, 11.44779295918254469 ) ) ;
#29824=CARTESIAN_POINT ( 'NONE',  ( 20.41236503877875563, 1.188189311754236144, -1.500000000000002220 ) ) ;
#29826=ORIENTED_EDGE ( 'NONE', *, *, #76437, .T. ) ;
#29827=EDGE_LOOP ( 'NONE', ( #90988, #30742, #26265, #27500 ) ) ;
#29829=ORIENTED_EDGE ( 'NONE', *, *, #49224, .T. ) ;
#29830=CARTESIAN_POINT ( 'NONE',  ( 19.44587849558928738, -12.39355811350142922, -1.500000000000002220 ) ) ;
#29832=CARTESIAN_POINT ( 'NONE',  ( 9.769481717609929561, -17.74358427669893956, -1.500000000000002220 ) ) ;
#29834=EDGE_CURVE ( 'NONE', #40387, #11406, #10943, .T. ) ;
#29835=CARTESIAN_POINT ( 'NONE',  ( -29.62287096154833677, -23.39681786206389447, 11.44779298504227860 ) ) ;
#29837=CARTESIAN_POINT ( 'NONE',  ( -40.67072903602026201, -25.30386692762919409, 5.536616400695820950 ) ) ;
#29839=CARTESIAN_POINT ( 'NONE',  ( -115.6228709571500559, -29.50249982740957577, 7.747779886224967605 ) ) ;
#29840=CARTESIAN_POINT ( 'NONE',  ( -99.55026156597334364, -24.35071581493543746, 9.817618358456025263 ) ) ;
#29841=CARTESIAN_POINT ( 'NONE',  ( 6.977786103627443559, 20.27319509581574408, 11.49999999999999645 ) ) ;
#29843=PLANE ( 'NONE',  #35515 ) ;
#29844=CARTESIAN_POINT ( 'NONE',  ( -61.58320691632388133, -24.51419770103157347, 9.386484678747178734 ) ) ;
#29845=ADVANCED_FACE ( 'NONE', ( #44640 ), #62367, .F. ) ;
#29846=ORIENTED_EDGE ( 'NONE', *, *, #50529, .F. ) ;
#29847=CARTESIAN_POINT ( 'NONE',  ( 12.98984941077313415, -16.12360325096057423, 11.49999999999998934 ) ) ;
#29848=CARTESIAN_POINT ( 'NONE',  ( -80.55620429048339304, -23.48783264082478084, -1.443836473390065045 ) ) ;
#29850=CARTESIAN_POINT ( 'NONE',  ( -28.52992191804173316, -24.35265584445642517, 0.6176551810875480220 ) ) ;
#29851=ORIENTED_EDGE ( 'NONE', *, *, #9450, .T. ) ;
#29855=CARTESIAN_POINT ( 'NONE',  ( 21.59112034314636119, 3.954845139028329015, 11.49999999999999645 ) ) ;
#29856=CARTESIAN_POINT ( 'NONE',  ( -91.52287095715006160, -24.65952944569304606, 1.056160979905700570 ) ) ;
#29857=CARTESIAN_POINT ( 'NONE',  ( 8.566404662457630437, 20.85315857434707709, -1.500000000000002220 ) ) ;
#29858=CARTESIAN_POINT ( 'NONE',  ( -5.413507703253908510, 20.27406835261982465, 11.49999999999998934 ) ) ;
#29859=CARTESIAN_POINT ( 'NONE',  ( -78.52287095715006160, -29.50248528299804818, 1.056150453629038477 ) ) ;
#29861=ORIENTED_EDGE ( 'NONE', *, *, #1330, .T. ) ;
#29863=EDGE_LOOP ( 'NONE', ( #95270, #25746, #96570, #47813 ) ) ;
#29864=ORIENTED_EDGE ( 'NONE', *, *, #86761, .F. ) ;
#29865=B_SPLINE_CURVE_WITH_KNOTS ( 'NONE', 3,
 ( #91587, #23057, #2137, #46418, #22067, #99194 ),
 .UNSPECIFIED., .F., .F.,
 ( 4, 2, 4 ),
 ( 0.000000000000000000, 0.001380764517854766267, 0.002761529035709532533 ),
 .UNSPECIFIED. ) ;
#29866=CARTESIAN_POINT ( 'NONE',  ( -66.58369449947565499, -24.51314013834316441, 0.6176544820404136216 ) ) ;
#29867=AXIS2_PLACEMENT_3D ( 'NONE', #87718, #975, #86704 ) ;
#29868=EDGE_CURVE ( 'NONE', #29958, #24375, #99893, .T. ) ;
#29869=CARTESIAN_POINT ( 'NONE',  ( 13.04721882220160012, 17.14300067834640373, -1.500000000000002220 ) ) ;
#29870=CARTESIAN_POINT ( 'NONE',  ( -121.5562042904833930, -24.66019654487199730, 8.947790411086121054 ) ) ;
#29871=ORIENTED_EDGE ( 'NONE', *, *, #38839, .T. ) ;
#29872=CARTESIAN_POINT ( 'NONE',  ( 9.660767377612277329, -18.76748907076374095, 11.49999999999998934 ) ) ;
#29875=CARTESIAN_POINT ( 'NONE',  ( -83.63279613814142976, -24.15620529776628089, 10.23563542870660470 ) ) ;
#29878=CARTESIAN_POINT ( 'NONE',  ( 21.58644828898399481, -4.983269013152989757, -1.500000000000002220 ) ) ;
#29879=FACE_OUTER_BOUND ( 'NONE', #5911, .T. ) ;
#29880=EDGE_CURVE ( 'NONE', #34688, #11149, #40060, .T. ) ;
#29882=ORIENTED_EDGE ( 'NONE', *, *, #75688, .T. ) ;
#29883=CARTESIAN_POINT ( 'NONE',  ( -51.93075163254042792, -25.31633345791246725, 6.142474900134158311 ) ) ;
#29884=CARTESIAN_POINT ( 'NONE',  ( -67.52287095715006160, -24.64898659630528854, 1.056161002820824368 ) ) ;
#29886=EDGE_CURVE ( 'NONE', #88628, #4409, #70238, .T. ) ;
#29887=CARTESIAN_POINT ( 'NONE',  ( -58.55620429048337883, -23.47593901973091235, -1.443836447539007972 ) ) ;
#29888=B_SPLINE_CURVE_WITH_KNOTS ( 'NONE', 3,
 ( #94794, #25787, #47639, #9062, #79066, #2460, #56762, #62360 ),
 .UNSPECIFIED., .F., .F.,
 ( 4, 2, 2, 4 ),
 ( -0.001240666984355838671, -0.0002401179793394966292, 0.0007604310256768454131, 0.002761529035709529498 ),
 .UNSPECIFIED. ) ;
#29889=CARTESIAN_POINT ( 'NONE',  ( -17.22176335520693158, -9.073154711715998744, -1.500000000000002220 ) ) ;
#29890=CARTESIAN_POINT ( 'NONE',  ( 8.370372042246325250, 19.68514866842044242, 11.49999999999998934 ) ) ;
#29891=CARTESIAN_POINT ( 'NONE',  ( -62.63696836751751817, -24.15543982623907482, -0.2315651400026649265 ) ) ;
#29892=FACE_OUTER_BOUND ( 'NONE', #20025, .T. ) ;
#29895=CARTESIAN_POINT ( 'NONE',  ( 18.72737137862276313, -12.84423604280260278, -1.500000000000002220 ) ) ;
#29896=EDGE_LOOP ( 'NONE', ( #57078, #29916, #26662, #99937 ) ) ;
#29897=DIRECTION ( 'NONE',  ( -3.773278334453079030E-23, 0.9999999999976377785, 2.173523156925979128E-06 ) ) ;
#29898=CARTESIAN_POINT ( 'NONE',  ( -62.62287095715002039, -23.96177878511307568, 10.65340807706330573 ) ) ;
#29899=CARTESIAN_POINT ( 'NONE',  ( 1.944447714513537262, -19.71154682592685958, 11.49999999999999645 ) ) ;
#29900=FACE_OUTER_BOUND ( 'NONE', #2753, .T. ) ;
#29904=CARTESIAN_POINT ( 'NONE',  ( 21.43499300031224664, 3.042053824063517542, -1.500000000000002220 ) ) ;
#29905=CARTESIAN_POINT ( 'NONE',  ( -99.62287095715005592, -24.65952944569304961, 1.056160979905702124 ) ) ;
#29906=CARTESIAN_POINT ( 'NONE',  ( -18.22486019313910077, 6.713856318530649681, -1.500000000000002220 ) ) ;
#29907=CARTESIAN_POINT ( 'NONE',  ( -61.62287095715004881, -24.65952944569304606, 1.056160979905695907 ) ) ;
#29908=B_SPLINE_CURVE_WITH_KNOTS ( 'NONE', 3,
 ( #47410, #1240, #55025, #78337, #31169, #78831 ),
 .UNSPECIFIED., .F., .F.,
 ( 4, 2, 4 ),
 ( 1.570887131794176733E-05, 0.001396322306279758037, 0.002776935741241574537 ),
 .UNSPECIFIED. ) ;
#29909=CARTESIAN_POINT ( 'NONE',  ( -129.5228709571500758, -23.47596703998600631, 11.44779298504227683 ) ) ;
#29910=CARTESIAN_POINT ( 'NONE',  ( 10.49454761162020588, -16.79419365751139637, -1.500000000000002220 ) ) ;
#29911=VERTEX_POINT ( 'NONE', #21282 ) ;
#29913=CARTESIAN_POINT ( 'NONE',  ( -19.79944955726156763, -4.570829099900970860, 11.49999999999999645 ) ) ;
#29914=CARTESIAN_POINT ( 'NONE',  ( -80.54148221499259819, -24.73486907724918282, 1.287355809206963908 ) ) ;
#29916=ORIENTED_EDGE ( 'NONE', *, *, #25519, .F. ) ;
#29917=B_SPLINE_SURFACE_WITH_KNOTS ( 'NONE', 3, 3, ( 
 ( #27375, #27866, #50216, #50711 ),
 ( #43104, #36475, #89771, #81158 ),
 ( #51709, #52209, #44096, #6024 ),
 ( #81661, #75023, #82648, #12133 ),
 ( #74048, #5030, #4547, #5522 ),
 ( #57839, #58334, #35491, #51211 ),
 ( #67438, #97382, #58824, #90267 ) ),
 .UNSPECIFIED., .F., .F., .F.,
 ( 4, 3, 4 ),
 ( 4, 4 ),
 ( 0.7945040050992233649, 0.8970133687736494554, 0.9995227324480754350 ),
 ( 0.1095218282603019622, 0.1105851153589713504 ),
 .UNSPECIFIED. ) ;
#29918=CARTESIAN_POINT ( 'NONE',  ( -102.5109869284088120, -24.51419770103155926, 9.386484678747178734 ) ) ;
#29919=CARTESIAN_POINT ( 'NONE',  ( -95.52287095715009002, -24.51254535375847965, 9.355368624242132114 ) ) ;
#29920=CARTESIAN_POINT ( 'NONE',  ( -49.27237840819080361, -25.25214495137587178, 5.251752546777291641 ) ) ;
#29921=B_SPLINE_CURVE_WITH_KNOTS ( 'NONE', 3,
 ( #93326, #77595, #16206, #1997 ),
 .UNSPECIFIED., .F., .F.,
 ( 4, 4 ),
 ( 1.392605083940956291E-05, 0.002317294749888688596 ),
 .UNSPECIFIED. ) ;
#29922=CARTESIAN_POINT ( 'NONE',  ( -54.62287095715005592, -23.47593901973091235, -1.443836447539009749 ) ) ;
#29923=B_SPLINE_CURVE_WITH_KNOTS ( 'NONE', 3,
 ( #57206, #893, #1903, #47079 ),
 .UNSPECIFIED., .F., .F.,
 ( 4, 4 ),
 ( 0.9011434845044391517, 0.9101499157765544634 ),
 .UNSPECIFIED. ) ;
#29925=CARTESIAN_POINT ( 'NONE',  ( -4.751880754313710042, -19.48972053015312866, -1.500000000000002220 ) ) ;
#29926=CARTESIAN_POINT ( 'NONE',  ( -28.58953762381673513, -23.32889918787351036, -1.443835802988293171 ) ) ;
#29927=ORIENTED_EDGE ( 'NONE', *, *, #38650, .F. ) ;
#29928=CARTESIAN_POINT ( 'NONE',  ( -36.52287095715006870, -24.64898659630367916, 1.056161002820819261 ) ) ;
#29929=CARTESIAN_POINT ( 'NONE',  ( 12.20170062390598709, -19.39347807479101249, 11.49999999999999645 ) ) ;
#29930=FACE_OUTER_BOUND ( 'NONE', #88653, .T. ) ;
#29931=DIRECTION ( 'NONE',  ( -3.773278334444167020E-23, 1.000000000000000000, 0.000000000000000000 ) ) ;
#29935=CARTESIAN_POINT ( 'NONE',  ( -99.52764846858842418, -25.27419814425944011, 3.999772249604663710 ) ) ;
#29936=DIRECTION ( 'NONE',  ( 3.773278334444167608E-23, -1.000000000000000000, 0.000000000000000000 ) ) ;
#29937=EDGE_LOOP ( 'NONE', ( #5505, #38209, #46457, #68260 ) ) ;
#29938=EDGE_CURVE ( 'NONE', #41839, #61801, #88397, .T. ) ;
#29939=CARTESIAN_POINT ( 'NONE',  ( -20.32544160278596834, -1.370942541838689799, 11.49999999999998934 ) ) ;
#29940=EDGE_LOOP ( 'NONE', ( #46807, #42177, #39094, #11299 ) ) ;
#29942=CARTESIAN_POINT ( 'NONE',  ( 20.38051395842347802, -10.57019977742728578, 11.49999999999998934 ) ) ;
#29944=AXIS2_PLACEMENT_3D ( 'NONE', #4912, #43969, #41992 ) ;
#29945=ADVANCED_FACE ( 'NONE', ( #69969 ), #92301, .T. ) ;
#29946=ORIENTED_EDGE ( 'NONE', *, *, #55967, .F. ) ;
#29947=CARTESIAN_POINT ( 'NONE',  ( -38.62287095715005592, -24.50216790748097750, 0.6166512839513631494 ) ) ;
#29948=EDGE_CURVE ( 'NONE', #73248, #3648, #61814, .T. ) ;
#29949=CARTESIAN_POINT ( 'NONE',  ( -116.5228709571500474, -23.96177878511309345, 10.65340807706329507 ) ) ;
#29951=CARTESIAN_POINT ( 'NONE',  ( -40.62287095715004170, -24.51163499207175178, 0.6490370598554262571 ) ) ;
#29952=CARTESIAN_POINT ( 'NONE',  ( -20.53569570583907122, -5.550916044964551155, 11.49999999999999645 ) ) ;
#29953=ORIENTED_EDGE ( 'NONE', *, *, #3420, .F. ) ;
#29955=CARTESIAN_POINT ( 'NONE',  ( 8.998109643811913472, -20.30750954041392120, 11.49999999999998934 ) ) ;
#29956=B_SPLINE_CURVE_WITH_KNOTS ( 'NONE', 3,
 ( #70680, #84402, #1174, #53968, #55466, #78771 ),
 .UNSPECIFIED., .F., .F.,
 ( 4, 2, 4 ),
 ( 0.000000000000000000, 0.001380764517854762580, 0.002761529035709525161 ),
 .UNSPECIFIED. ) ;
#29957=CARTESIAN_POINT ( 'NONE',  ( 6.296002175621457475, 19.65409743616946514, -1.500000000000002220 ) ) ;
#29958=VERTEX_POINT ( 'NONE', #76072 ) ;
#29962=VERTEX_POINT ( 'NONE', #53257 ) ;
#29964=CARTESIAN_POINT ( 'NONE',  ( -127.1722388760373690, -25.27126041720325844, 4.079010001960287291 ) ) ;
#29966=CARTESIAN_POINT ( 'NONE',  ( 12.46380520747237419, 16.70348211664046900, -1.500000000000002220 ) ) ;
#29967=CARTESIAN_POINT ( 'NONE',  ( -8.041798833237560729, -20.28069125152608976, 11.49999999999999645 ) ) ;
#29970=CARTESIAN_POINT ( 'NONE',  ( -11.43049785330379997, -19.34545768653811493, -1.500000000000002220 ) ) ;
#29972=ORIENTED_EDGE ( 'NONE', *, *, #57170, .T. ) ;
#29973=FACE_OUTER_BOUND ( 'NONE', #62481, .T. ) ;
#29974=CARTESIAN_POINT ( 'NONE',  ( -57.55620429048338593, -24.65952944569304606, 1.056160979905696573 ) ) ;
#29975=EDGE_CURVE ( 'NONE', #34855, #58437, #68476, .T. ) ;
#29977=ORIENTED_EDGE ( 'NONE', *, *, #16319, .F. ) ;
#29980=VERTEX_POINT ( 'NONE', #14676 ) ;
#29981=CARTESIAN_POINT ( 'NONE',  ( 13.79380260783658407, 16.28676726024703214, -1.500000000000002220 ) ) ;
#29982=ORIENTED_EDGE ( 'NONE', *, *, #66132, .F. ) ;
#29984=CARTESIAN_POINT ( 'NONE',  ( -13.78326148797977169, 15.88460234914768421, -1.500000000000002220 ) ) ;
#29985=CARTESIAN_POINT ( 'NONE',  ( -30.59476385451626257, -24.83983788297006612, 1.633466014234818076 ) ) ;
#29986=CARTESIAN_POINT ( 'NONE',  ( -55.62287095715005592, -23.47593901973091235, -1.443836447539007972 ) ) ;
#29987=CARTESIAN_POINT ( 'NONE',  ( -56.52287095715006870, -29.50250786944525672, 11.44777988621623876 ) ) ;
#29988=CARTESIAN_POINT ( 'NONE',  ( -21.97012646571106842, -0.5360883523215664859, -1.500000000000002220 ) ) ;
#29989=CARTESIAN_POINT ( 'NONE',  ( -87.54805663165109308, -24.34968618360934656, 0.1864209137778970737 ) ) ;
#29991=CARTESIAN_POINT ( 'NONE',  ( -74.52287095715007581, -24.64965694238408034, 8.947790433994200043 ) ) ;
#29992=EDGE_CURVE ( 'NONE', #55686, #79917, #30343, .T. ) ;
#29993=CARTESIAN_POINT ( 'NONE',  ( -116.6228709571500559, -24.64898659630368627, 1.056161002820833028 ) ) ;
#29994=LINE ( 'NONE', #92392, #91118 ) ;
#29995=CARTESIAN_POINT ( 'NONE',  ( -20.41826355431054907, -23.96543168844442562, 8.640809912072075605 ) ) ;
#29996=CARTESIAN_POINT ( 'NONE',  ( 17.78463046036513617, -11.72987588014745342, 11.49999999999998934 ) ) ;
#29997=CARTESIAN_POINT ( 'NONE',  ( -75.52287095715007581, -29.50250243563736774, 8.947779886222141599 ) ) ;
#29998=CARTESIAN_POINT ( 'NONE',  ( -52.22287095715005734, -23.47596703998600276, 11.44779298504227683 ) ) ;
#29999=EDGE_CURVE ( 'NONE', #35212, #12246, #79947, .T. ) ;
#30001=CARTESIAN_POINT ( 'NONE',  ( -90.62287095715004170, -24.99132157543084531, 2.256160258750667502 ) ) ;
#30002=CARTESIAN_POINT ( 'NONE',  ( -33.60141147702453424, -23.96119346886880308, -0.6495511937832006977 ) ) ;
#30003=CARTESIAN_POINT ( 'NONE',  ( 15.63351008929417318, -16.12541905121107177, -1.500000000000002220 ) ) ;
#30004=CARTESIAN_POINT ( 'NONE',  ( -110.9395699835130813, -25.31476271379807841, 5.144092056987718209 ) ) ;
#30006=CARTESIAN_POINT ( 'NONE',  ( -99.43243614344049774, -25.11009041281529974, 7.230259461350549088 ) ) ;
#30007=CARTESIAN_POINT ( 'NONE',  ( 8.161054176536994831, -17.82452852192863091, 11.49999999999999645 ) ) ;
#30008=FACE_OUTER_BOUND ( 'NONE', #83795, .T. ) ;
#30012=CARTESIAN_POINT ( 'NONE',  ( -79.62287095715005592, -29.50250243563736774, 8.947779886222141599 ) ) ;
#30013=PLANE ( 'NONE',  #18846 ) ;
#30014=CARTESIAN_POINT ( 'NONE',  ( -90.93251974643131064, -25.31476272485208412, 5.144091107239472827 ) ) ;
#30017=CARTESIAN_POINT ( 'NONE',  ( -18.32884136524465291, -7.267937366463995907, 11.49999999999998934 ) ) ;
#30018=ORIENTED_EDGE ( 'NONE', *, *, #50288, .T. ) ;
#30019=CARTESIAN_POINT ( 'NONE',  ( -110.2103586364410290, -25.19572374053056407, 3.298817077610923132 ) ) ;
#30025=CARTESIAN_POINT ( 'NONE',  ( -55.63150118323845561, -24.73486907724917572, 1.287355809206962798 ) ) ;
#30026=CARTESIAN_POINT ( 'NONE',  ( -99.48801098274306298, -25.03145115913622121, 7.273530651135964753 ) ) ;
#30028=CARTESIAN_POINT ( 'NONE',  ( -70.74026866089610621, -25.31511106678998502, 4.894904372220056921 ) ) ;
#30029=CARTESIAN_POINT ( 'NONE',  ( -107.6339924380179980, -23.48783264082479505, -1.443836473390060826 ) ) ;
#30030=CARTESIAN_POINT ( 'NONE',  ( -19.61284664649099696, 3.773188449817356904, -1.500000000000002220 ) ) ;
#30031=CARTESIAN_POINT ( 'NONE',  ( -125.6228709571500559, -24.63345952396256422, 9.038047939301492306 ) ) ;
#30032=CARTESIAN_POINT ( 'NONE',  ( -45.55045081875104529, -24.15602025860896163, 10.28564288303535434 ) ) ;
#30038=CARTESIAN_POINT ( 'NONE',  ( -81.54383403257651253, -24.51314013834316796, 0.6176544820404249458 ) ) ;
#30039=B_SPLINE_CURVE_WITH_KNOTS ( 'NONE', 3,
 ( #90221, #51665, #82602, #44045 ),
 .UNSPECIFIED., .F., .F.,
 ( 4, 4 ),
 ( 0.000000000000000000, 0.002769230769239627420 ),
 .UNSPECIFIED. ) ;
#30040=CARTESIAN_POINT ( 'NONE',  ( -27.70544111104076990, -24.60093890412679229, 1.628749891592534693 ) ) ;
#30042=B_SPLINE_CURVE_WITH_KNOTS ( 'NONE', 3,
 ( #69259, #16456, #68764, #47928 ),
 .UNSPECIFIED., .F., .F.,
 ( 4, 4 ),
 ( 0.1506075451614858618, 0.1596139764336012845 ),
 .UNSPECIFIED. ) ;
#30043=CARTESIAN_POINT ( 'NONE',  ( -79.62287095715005592, -23.48786465467241058, 11.44779295918254469 ) ) ;
#30046=ADVANCED_FACE ( 'NONE', ( #41034 ), #23789, .T. ) ;
#30047=CARTESIAN_POINT ( 'NONE',  ( -9.609455416251792670, -17.83980533922896683, -1.500000000000002220 ) ) ;
#30048=CARTESIAN_POINT ( 'NONE',  ( -76.62287095715007013, -23.48786465467241058, 11.44779295918254469 ) ) ;
#30051=CARTESIAN_POINT ( 'NONE',  ( -90.52287095715007581, -24.82558206586149652, 1.605769216559628010 ) ) ;
#30052=EDGE_CURVE ( 'NONE', #24726, #81664, #38781, .T. ) ;
#30055=B_SPLINE_CURVE_WITH_KNOTS ( 'NONE', 3,
 ( #88462, #10331, #63640, #10835 ),
 .UNSPECIFIED., .F., .F.,
 ( 4, 4 ),
 ( 1.422342543128534982E-05, 0.002384588281187964391 ),
 .UNSPECIFIED. ) ;
#30057=CARTESIAN_POINT ( 'NONE',  ( 19.44710440357065551, 5.058846670610233076, -1.500000000000002220 ) ) ;
#30059=CARTESIAN_POINT ( 'NONE',  ( 15.50021099394596646, 14.30638080151107694, 11.49999999999999645 ) ) ;
#30061=CARTESIAN_POINT ( 'NONE',  ( 19.10104996495751450, -11.12853483292915691, -1.500000000000002220 ) ) ;
#30062=EDGE_CURVE ( 'NONE', #26538, #85004, #2317, .T. ) ;
#30063=CARTESIAN_POINT ( 'NONE',  ( 12.93548710985481698, 15.95582723538240266, -1.500000000000002220 ) ) ;
#30064=CARTESIAN_POINT ( 'NONE',  ( -47.52287095715006160, -23.47596703998600631, 11.44779298504229104 ) ) ;
#30065=VECTOR ( 'NONE', #13341, 1000.000000000000227 ) ;
#30066=CARTESIAN_POINT ( 'NONE',  ( -60.55145188000605572, -24.15503026093916006, -0.2815557561904390993 ) ) ;
#30067=ORIENTED_EDGE ( 'NONE', *, *, #12659, .T. ) ;
#30068=DIRECTION ( 'NONE',  ( 0.000000000000000000, -2.173523156925980399E-06, 0.9999999999976378895 ) ) ;
#30069=VERTEX_POINT ( 'NONE', #70477 ) ;
#30070=CARTESIAN_POINT ( 'NONE',  ( -100.3561995057198288, -25.12094576395124790, 2.834877649516965636 ) ) ;
#30071=CARTESIAN_POINT ( 'NONE',  ( -87.62287095715004170, -24.66019654487199020, 8.947790411086129936 ) ) ;
#30073=VERTEX_POINT ( 'NONE', #24298 ) ;
#30076=CARTESIAN_POINT ( 'NONE',  ( -80.72727431975152967, -25.25269385731764160, 3.802325930818207134 ) ) ;
#30077=LINE ( 'NONE', #99082, #81048 ) ;
#30078=FACE_OUTER_BOUND ( 'NONE', #83765, .T. ) ;
#30079=ADVANCED_FACE ( 'NONE', ( #961 ), #65340, .T. ) ;
#30080=CARTESIAN_POINT ( 'NONE',  ( 15.34805171112899203, -13.82090413600154299, -1.500000000000002220 ) ) ;
#30082=CARTESIAN_POINT ( 'NONE',  ( -12.93760099376155104, 17.33828479246177423, 11.49999999999999645 ) ) ;
#30083=ORIENTED_EDGE ( 'NONE', *, *, #23881, .T. ) ;
#30084=DIRECTION ( 'NONE',  ( -3.773278334453079618E-23, 0.9999999999976377785, 2.173523156925979975E-06 ) ) ;
#30085=CARTESIAN_POINT ( 'NONE',  ( -96.62287095715005592, -24.64965695001468404, 8.947790433994178727 ) ) ;
#30086=CARTESIAN_POINT ( 'NONE',  ( -20.28323820415832657, -9.445149539555593776, 11.49999999999998934 ) ) ;
#30088=CARTESIAN_POINT ( 'NONE',  ( -62.52287095715006160, -23.73907113216987952, -1.053371485793251461 ) ) ;
#30089=CARTESIAN_POINT ( 'NONE',  ( -82.52287095715006160, -23.47593901973090169, -1.443836447538996648 ) ) ;
#30090=ORIENTED_EDGE ( 'NONE', *, *, #92299, .T. ) ;
#30093=CARTESIAN_POINT ( 'NONE',  ( -12.66259425867894350, -16.64798919286708667, -1.500000000000002220 ) ) ;
#30094=ORIENTED_EDGE ( 'NONE', *, *, #27326, .T. ) ;
#30095=CARTESIAN_POINT ( 'NONE',  ( -67.51046660421201295, -23.96169478059713853, 10.65365249895717881 ) ) ;
#30098=CARTESIAN_POINT ( 'NONE',  ( -109.6310424504063974, -23.73791477778912551, 11.05961554403169878 ) ) ;
#30099=CARTESIAN_POINT ( 'NONE',  ( 16.79009078985406234, 12.93418496121567252, -1.500000000000002220 ) ) ;
#30100=EDGE_LOOP ( 'NONE', ( #91952, #99901, #17869, #22880 ) ) ;
#30102=CARTESIAN_POINT ( 'NONE',  ( -99.97649549088345111, -25.12215660189515631, 7.032284957836063555 ) ) ;
#30103=CARTESIAN_POINT ( 'NONE',  ( 13.71991279636371175, 16.93377936151356877, 11.49999999999998934 ) ) ;
#30105=CARTESIAN_POINT ( 'NONE',  ( -35.58953762381672448, -24.99156044556202616, 7.747789690856173195 ) ) ;
#30107=CARTESIAN_POINT ( 'NONE',  ( 21.40858030128615397, -3.853468400179685727, -1.500000000000002220 ) ) ;
#30109=CARTESIAN_POINT ( 'NONE',  ( -18.48265707593502327, -12.51853143457666562, 11.49999999999999645 ) ) ;
#30114=CARTESIAN_POINT ( 'NONE',  ( -43.62287095715006302, -24.33832256526967797, 0.1851278514119845120 ) ) ;
#30115=EDGE_LOOP ( 'NONE', ( #33573, #35870, #97987, #95439 ) ) ;
#30116=ORIENTED_EDGE ( 'NONE', *, *, #59512, .T. ) ;
#30119=CARTESIAN_POINT ( 'NONE',  ( 21.18767802922067034, -0.7184367399587067160, -1.500000000000002220 ) ) ;
#30121=CARTESIAN_POINT ( 'NONE',  ( -80.29067095681661215, -25.03138296994456979, 7.551389794076908579 ) ) ;
#30124=CARTESIAN_POINT ( 'NONE',  ( -19.24332624019526961, -2.196797614219411443, -1.500000000000002220 ) ) ;
#30125=ADVANCED_FACE ( 'NONE', ( #69800 ), #100215, .F. ) ;
#30126=CARTESIAN_POINT ( 'NONE',  ( -45.52197100924568218, -23.48783264082476308, -1.443836473390102793 ) ) ;
#30128=CARTESIAN_POINT ( 'NONE',  ( 1.664315604108443925, 19.36118569274438528, 11.49999999999999645 ) ) ;
#30129=CARTESIAN_POINT ( 'NONE',  ( -107.9228709571500815, -23.47596703998600631, 11.44779298504227860 ) ) ;
#30130=B_SPLINE_CURVE_WITH_KNOTS ( 'NONE', 3,
 ( #69625, #68127, #99049, #22908 ),
 .UNSPECIFIED., .F., .F.,
 ( 4, 4 ),
 ( 0.000000000000000000, 9.999999999998897304E-05 ),
 .UNSPECIFIED. ) ;
#30132=ORIENTED_EDGE ( 'NONE', *, *, #20604, .T. ) ;
#30135=VECTOR ( 'NONE', #67751, 1000.000000000000114 ) ;
#30136=CARTESIAN_POINT ( 'NONE',  ( -97.25593102651548350, -24.04668586515358442, 10.47594215909545312 ) ) ;
#30137=CARTESIAN_POINT ( 'NONE',  ( 18.70796670040472165, 5.986831462552164140, -1.500000000000002220 ) ) ;
#30138=CARTESIAN_POINT ( 'NONE',  ( -41.23075053442405391, -25.27806068830949116, 4.755616919394483055 ) ) ;
#30140=CARTESIAN_POINT ( 'NONE',  ( 20.54099941694853726, 6.510794959084822864, -1.500000000000002220 ) ) ;
#30143=CARTESIAN_POINT ( 'NONE',  ( -99.56269727232219680, -25.27473330506526139, 3.795001076773547144 ) ) ;
#30144=CARTESIAN_POINT ( 'NONE',  ( -21.01138170180016118, -9.542296329091309204, -1.500000000000002220 ) ) ;
#30149=CARTESIAN_POINT ( 'NONE',  ( -89.22287095715005023, -23.47596703998600631, 11.44779298504227860 ) ) ;
#30150=CARTESIAN_POINT ( 'NONE',  ( 7.037473118728134303, -18.94123407977296480, 11.49999999999999645 ) ) ;
#30151=CARTESIAN_POINT ( 'NONE',  ( -121.5198912994663232, -24.15620529776628800, 10.23563542870660115 ) ) ;
#30152=LINE ( 'NONE', #83439, #30599 ) ;
#30155=CARTESIAN_POINT ( 'NONE',  ( -111.7788625685672486, -25.29824125544099900, 4.278827553184073373 ) ) ;
#30156=DIRECTION ( 'NONE',  ( -1.000000000000000000, -3.773278334444166432E-23, -8.201307841325785021E-29 ) ) ;
#30157=CARTESIAN_POINT ( 'NONE',  ( -110.8177083405623478, -25.18425605443559689, 3.398758359099868009 ) ) ;
#30158=CARTESIAN_POINT ( 'NONE',  ( 19.88832268942539017, -0.5522253751840191516, -1.500000000000002220 ) ) ;
#30160=CARTESIAN_POINT ( 'NONE',  ( -79.11611000704996854, -25.19045605819419720, 3.255062319851647956 ) ) ;
#30161=CARTESIAN_POINT ( 'NONE',  ( 3.553741186906278493, -19.43417129498564577, -1.500000000000002220 ) ) ;
#30164=CARTESIAN_POINT ( 'NONE',  ( -123.5228709571500616, -23.47596703998600631, 11.44779298504227860 ) ) ;
#30165=CARTESIAN_POINT ( 'NONE',  ( -42.52287095715005449, -24.64898659630367206, 1.056161002820819261 ) ) ;
#30166=CARTESIAN_POINT ( 'NONE',  ( -19.97286373971314433, -5.326668811655218327, 11.49999999999999645 ) ) ;
#30167=CARTESIAN_POINT ( 'NONE',  ( -128.5228709571500758, -24.64965694238575722, 8.947790433994189385 ) ) ;
#30168=CARTESIAN_POINT ( 'NONE',  ( -49.95596087352405590, -25.25138688028978962, 5.268391457946761669 ) ) ;
#30169=CARTESIAN_POINT ( 'NONE',  ( -10.65177407370799045, -20.06881281718593613, 11.49999999999999645 ) ) ;
#30170=ORIENTED_EDGE ( 'NONE', *, *, #43649, .F. ) ;
#30171=CARTESIAN_POINT ( 'NONE',  ( -39.52287095715006870, -29.50250243563736774, 8.947779886222148704 ) ) ;
#30172=CARTESIAN_POINT ( 'NONE',  ( -69.34919748320460542, -25.23279835387202397, 6.332189406089158368 ) ) ;
#30173=CARTESIAN_POINT ( 'NONE',  ( -19.70923665959843873, 4.302044407003456250, 11.49999999999998934 ) ) ;
#30174=CARTESIAN_POINT ( 'NONE',  ( -63.50973006361228101, -23.96119346886879597, -0.6495511937832106897 ) ) ;
#30175=CARTESIAN_POINT ( 'NONE',  ( -100.4326965455115044, -29.50249014687182836, 3.293933732389337621 ) ) ;
#30177=ORIENTED_EDGE ( 'NONE', *, *, #26180, .F. ) ;
#30178=ORIENTED_EDGE ( 'NONE', *, *, #6637, .T. ) ;
#30180=CARTESIAN_POINT ( 'NONE',  ( -4.124250913864588419, 22.51598698906299845, 11.49999999999998934 ) ) ;
#30181=CARTESIAN_POINT ( 'NONE',  ( -50.90914965406638260, -25.18439674812242401, 3.408962482538700378 ) ) ;
#30182=CARTESIAN_POINT ( 'NONE',  ( -21.34238180412542718, 3.497892552127677135, -1.500000000000002220 ) ) ;
#30183=CARTESIAN_POINT ( 'NONE',  ( -123.6253769750481837, -23.96119346886881019, -0.6495511937832022520 ) ) ;
#30184=CARTESIAN_POINT ( 'NONE',  ( -34.66745945777220328, -23.48783264082478084, -1.443836473390076591 ) ) ;
#30186=CARTESIAN_POINT ( 'NONE',  ( -18.75169668496848985, 9.291489096422434812, 11.49999999999999645 ) ) ;
#30187=ORIENTED_EDGE ( 'NONE', *, *, #10590, .T. ) ;
#30188=CARTESIAN_POINT ( 'NONE',  ( -68.96115101070704156, -25.24754476957743066, 5.914983662711241763 ) ) ;
#30189=CARTESIAN_POINT ( 'NONE',  ( -2.902263480631018577, 21.84654903556016947, -1.500000000000002220 ) ) ;
#30190=EDGE_CURVE ( 'NONE', #42367, #96258, #39859, .T. ) ;
#30191=CARTESIAN_POINT ( 'NONE',  ( -61.62287095715004881, -29.50250243563736774, 8.947779886222145151 ) ) ;
#30192=CARTESIAN_POINT ( 'NONE',  ( -28.29841854899664710, -24.79700284414744615, 7.453535061713724374 ) ) ;
#30193=ORIENTED_EDGE ( 'NONE', *, *, #48715, .T. ) ;
#30195=CARTESIAN_POINT ( 'NONE',  ( -90.54023306201428056, -25.00182538069146787, 7.747789668545043362 ) ) ;
#30198=ORIENTED_EDGE ( 'NONE', *, *, #55648, .T. ) ;
#30200=CARTESIAN_POINT ( 'NONE',  ( -71.60197075763308305, -23.73791477778911840, 11.05961554403170766 ) ) ;
#30201=DIRECTION ( 'NONE',  ( -3.773278334453079030E-23, 0.9999999999976377785, 2.173523156925979128E-06 ) ) ;
#30202=CARTESIAN_POINT ( 'NONE',  ( -81.62287095715005592, -24.64898659630528854, 1.056161002820826145 ) ) ;
#30204=CARTESIAN_POINT ( 'NONE',  ( 20.49162120248849561, -0.4999214236376636200, -1.500000000000002220 ) ) ;
#30205=VERTEX_POINT ( 'NONE', #37362 ) ;
#30207=CARTESIAN_POINT ( 'NONE',  ( -30.61275986115374081, -24.37728322581795481, 9.960208392924579712 ) ) ;
#30208=CARTESIAN_POINT ( 'NONE',  ( -56.62287095715005592, -24.64898659630528499, 1.056161002820822592 ) ) ;
#30209=CARTESIAN_POINT ( 'NONE',  ( -4.481184387785930312, -21.81124396384582909, -1.500000000000002220 ) ) ;
#30212=CARTESIAN_POINT ( 'NONE',  ( -88.62287095715005592, -24.35013146730204170, 9.818937971375104823 ) ) ;
#30214=CARTESIAN_POINT ( 'NONE',  ( -85.52287095715006160, -29.50248528299804818, 1.056150453629040253 ) ) ;
#30216=CARTESIAN_POINT ( 'NONE',  ( 9.628234360240019996, 18.42577530400075858, -1.500000000000002220 ) ) ;
#30220=VECTOR ( 'NONE', #58898, 1000.000000000000114 ) ;
#30221=CARTESIAN_POINT ( 'NONE',  ( -118.9228709571500673, -23.47596703998600631, 11.44779298504227683 ) ) ;
#30223=ORIENTED_EDGE ( 'NONE', *, *, #70633, .F. ) ;
#30225=CARTESIAN_POINT ( 'NONE',  ( -53.62287095715005592, -29.50250243563736774, 8.947779886222146928 ) ) ;
#30227=CARTESIAN_POINT ( 'NONE',  ( -59.62287095715006302, -23.48786465467241058, 11.44779295918254824 ) ) ;
#30228=VECTOR ( 'NONE', #79761, 1000.000000000000114 ) ;
#30230=CARTESIAN_POINT ( 'NONE',  ( -110.5228709571500758, -23.84047902841603772, -0.8780736468305414544 ) ) ;
#30231=DIRECTION ( 'NONE',  ( 3.773278334444166432E-23, -1.000000000000000000, 0.000000000000000000 ) ) ;
#30232=CARTESIAN_POINT ( 'NONE',  ( -0.8124730928778809425, -22.15030348749839817, 11.49999999999999645 ) ) ;
#30233=ORIENTED_EDGE ( 'NONE', *, *, #88271, .T. ) ;
#30234=FACE_OUTER_BOUND ( 'NONE', #13015, .T. ) ;
#30235=CARTESIAN_POINT ( 'NONE',  ( 18.27610663105864219, 13.37729726205769154, 11.49999999999998934 ) ) ;
#30237=CARTESIAN_POINT ( 'NONE',  ( -124.5895376238167245, -23.47593901973091235, -1.443836447538997536 ) ) ;
#30238=VERTEX_POINT ( 'NONE', #31735 ) ;
#30240=ORIENTED_EDGE ( 'NONE', *, *, #6420, .F. ) ;
#30241=CARTESIAN_POINT ( 'NONE',  ( -110.5228709571500616, -23.47596703998600631, 11.44779298504228038 ) ) ;
#30242=EDGE_CURVE ( 'NONE', #88518, #28525, #7386, .T. ) ;
#30243=CARTESIAN_POINT ( 'NONE',  ( 9.271505649751263789, 17.87650053469100087, 11.49999999999998934 ) ) ;
#30244=CARTESIAN_POINT ( 'NONE',  ( -99.52287095715006160, -23.47596703998600631, 11.44779298504228215 ) ) ;
#30245=EDGE_LOOP ( 'NONE', ( #38052, #16095, #68930, #36856 ) ) ;
#30247=CARTESIAN_POINT ( 'NONE',  ( 9.556255610625576935, 20.19728179944524271, -1.500000000000002220 ) ) ;
#30248=ORIENTED_EDGE ( 'NONE', *, *, #3732, .T. ) ;
#30249=EDGE_LOOP ( 'NONE', ( #37416, #85241, #28110, #29215 ) ) ;
#30250=CARTESIAN_POINT ( 'NONE',  ( -44.52287095715006160, -29.50250243563736774, 8.947779886222148704 ) ) ;
#30251=PLANE ( 'NONE',  #86417 ) ;
#30252=CARTESIAN_POINT ( 'NONE',  ( -80.35919894935767616, -25.29542306156489673, 4.505481338088394239 ) ) ;
#30254=DIRECTION ( 'NONE',  ( 0.000000000000000000, -0.9999999999976377785, -2.173523156925979128E-06 ) ) ;
#30255=DIRECTION ( 'NONE',  ( -3.773278334453079030E-23, 0.9999999999976377785, 2.173523156925979128E-06 ) ) ;
#30256=B_SPLINE_CURVE_WITH_KNOTS ( 'NONE', 3,
 ( #99151, #59620, #98151, #4334 ),
 .UNSPECIFIED., .F., .F.,
 ( 4, 4 ),
 ( 0.000000000000000000, 9.999999999997510880E-05 ),
 .UNSPECIFIED. ) ;
#30257=CARTESIAN_POINT ( 'NONE',  ( 18.72186718581493636, -5.619560887262019300, 11.49999999999998934 ) ) ;
#30258=CARTESIAN_POINT ( 'NONE',  ( -50.38191529551148307, -25.11033443737753146, 2.832404817301930056 ) ) ;
#30259=CARTESIAN_POINT ( 'NONE',  ( 2.695732861974529104, -21.29187259674557708, -1.500000000000002220 ) ) ;
#30263=CARTESIAN_POINT ( 'NONE',  ( -129.5228709571500758, -24.35013146730204525, 9.818937971375099494 ) ) ;
#30264=CARTESIAN_POINT ( 'NONE',  ( 22.79674358141071977, 1.614764915196592598, -1.500000000000002220 ) ) ;
#30265=EDGE_CURVE ( 'NONE', #37127, #34684, #27824, .T. ) ;
#30268=CARTESIAN_POINT ( 'NONE',  ( -96.56113353449998726, -23.48786465467241413, 11.44779295918254469 ) ) ;
#30270=CARTESIAN_POINT ( 'NONE',  ( 19.27460657395150889, -5.330843762518559181, 11.49999999999999645 ) ) ;
#30273=CARTESIAN_POINT ( 'NONE',  ( -108.6228709571500701, -24.50216790748099882, 0.6166512839513758060 ) ) ;
#30274=ORIENTED_EDGE ( 'NONE', *, *, #11053, .T. ) ;
#30275=CARTESIAN_POINT ( 'NONE',  ( -89.55620429048337883, -24.64898659630528854, 1.056161002820830364 ) ) ;
#30277=CARTESIAN_POINT ( 'NONE',  ( -3.653784360050144286, 21.42803128968991544, 11.49999999999998934 ) ) ;
#30279=CARTESIAN_POINT ( 'NONE',  ( -34.52287095715004739, -24.66019654487199730, 8.947790411086121054 ) ) ;
#30280=CARTESIAN_POINT ( 'NONE',  ( 19.59400933563812330, 0.1774559437341752532, -1.500000000000002220 ) ) ;
#30283=DIRECTION ( 'NONE',  ( 0.000000000000000000, -0.9999999999976377785, -2.173523156925979128E-06 ) ) ;
#30285=DIRECTION ( 'NONE',  ( -3.773278334444167608E-23, 1.000000000000000000, 0.000000000000000000 ) ) ;
#30287=CARTESIAN_POINT ( 'NONE',  ( -5.951451697817415010, -19.63005813332872762, 11.49999999999999645 ) ) ;
#30291=VERTEX_POINT ( 'NONE', #93121 ) ;
#30292=CARTESIAN_POINT ( 'NONE',  ( -62.52287095715006160, -23.47596703998600631, 11.44779298504228926 ) ) ;
#30293=DIRECTION ( 'NONE',  ( -3.773278334453079030E-23, 0.9999999999976377785, 2.173523156925979128E-06 ) ) ;
#30295=CARTESIAN_POINT ( 'NONE',  ( -125.5215403751119538, -23.85049219812686871, 10.88485053497526778 ) ) ;
#30298=EDGE_CURVE ( 'NONE', #21630, #88472, #8412, .T. ) ;
#30299=EDGE_CURVE ( 'NONE', #41257, #37557, #79743, .T. ) ;
#30302=CARTESIAN_POINT ( 'NONE',  ( 14.79121776280621425, -17.69394282334246427, 11.49999999999999645 ) ) ;
#30303=CARTESIAN_POINT ( 'NONE',  ( 22.80427751693360960, 0.003464389817739472934, -1.500000000000002220 ) ) ;
#30304=CARTESIAN_POINT ( 'NONE',  ( -104.5228709571500758, -23.72747288104470798, -1.053458166803225460 ) ) ;
#30305=CARTESIAN_POINT ( 'NONE',  ( -75.52287095715004739, -24.91570333825771399, 8.075032458260347212 ) ) ;
#30306=CARTESIAN_POINT ( 'NONE',  ( -123.5228709571501469, -23.73907113216990439, -1.053371485793244799 ) ) ;
#30307=CARTESIAN_POINT ( 'NONE',  ( 1.926536275058113867, -22.33200895297504474, 11.49999999999999645 ) ) ;
#30308=FACE_OUTER_BOUND ( 'NONE', #23290, .T. ) ;
#30309=CARTESIAN_POINT ( 'NONE',  ( -99.25999413675920380, -25.31582255457039921, 5.189783737494863658 ) ) ;
#30310=CARTESIAN_POINT ( 'NONE',  ( -21.91604229967229500, -0.6759211909499470705, -1.500000000000002220 ) ) ;
#30313=CARTESIAN_POINT ( 'NONE',  ( -85.52287095715004739, -29.50248789122583659, 2.256150453626215580 ) ) ;
#30314=CARTESIAN_POINT ( 'NONE',  ( -125.6228709571500559, -29.50250243563736774, 8.947779886222132717 ) ) ;
#30316=CARTESIAN_POINT ( 'NONE',  ( -48.88075183786669697, -25.23570012922559158, 6.306895103940420633 ) ) ;
#30317=DIRECTION ( 'NONE',  ( -3.773278334453079030E-23, 0.9999999999976377785, 2.173523156925979128E-06 ) ) ;
#30318=ORIENTED_EDGE ( 'NONE', *, *, #776, .F. ) ;
#30319=CARTESIAN_POINT ( 'NONE',  ( 6.539103723289373171, -19.38406401830294712, 11.49999999999998934 ) ) ;
#30320=ORIENTED_EDGE ( 'NONE', *, *, #23641, .F. ) ;
#30321=B_SPLINE_CURVE_WITH_KNOTS ( 'NONE', 3,
 ( #55039, #31691, #62659, #94083, #9346, #93574 ),
 .UNSPECIFIED., .F., .F.,
 ( 4, 2, 4 ),
 ( 1.570755371633895505E-05, 0.001396183895866086669, 0.002776660238015834278 ),
 .UNSPECIFIED. ) ;
#30322=VERTEX_POINT ( 'NONE', #98767 ) ;
#30324=VERTEX_POINT ( 'NONE', #6433 ) ;
#30325=CARTESIAN_POINT ( 'NONE',  ( -23.05830607064937965, -0.9945063503333604338, -1.500000000000002220 ) ) ;
#30326=CARTESIAN_POINT ( 'NONE',  ( -61.62365984720521794, -24.65952944569304961, 1.056160979905699682 ) ) ;
#30327=ADVANCED_FACE ( 'NONE', ( #37387 ), #14532, .F. ) ;
#30328=CARTESIAN_POINT ( 'NONE',  ( -19.75413285895528404, 4.560271753130525241, -1.500000000000002220 ) ) ;
#30329=VERTEX_POINT ( 'NONE', #60237 ) ;
#30331=CARTESIAN_POINT ( 'NONE',  ( -28.20733355685459642, -25.00894895108924842, 3.118813907533751983 ) ) ;
#30332=CARTESIAN_POINT ( 'NONE',  ( -87.62287095715007013, -23.73934037231757443, 11.05740245334328797 ) ) ;
#30334=DIRECTION ( 'NONE',  ( -3.773278334453079030E-23, 0.9999999999976377785, 2.173523156925979128E-06 ) ) ;
#30335=CARTESIAN_POINT ( 'NONE',  ( -70.58916620125799568, -24.52300882791528380, 0.6510814631126248253 ) ) ;
#30336=CARTESIAN_POINT ( 'NONE',  ( 18.29419249859179786, 11.19154738541161365, 11.49999999999999645 ) ) ;
#30338=CARTESIAN_POINT ( 'NONE',  ( -113.6228709571500559, -24.50216790748099527, 0.6166512839513743627 ) ) ;
#30339=CARTESIAN_POINT ( 'NONE',  ( -110.9228709571500673, -23.47593901973090524, -1.443836447538996426 ) ) ;
#30342=CARTESIAN_POINT ( 'NONE',  ( -14.56105648253378781, -14.73650127990469016, 11.49999999999998934 ) ) ;
#30343=B_SPLINE_CURVE_WITH_KNOTS ( 'NONE', 3,
 ( #7570, #70982, #16179, #10072, #1472, #32917 ),
 .UNSPECIFIED., .F., .F.,
 ( 4, 2, 4 ),
 ( 0.000000000000000000, 0.001380901958385395483, 0.002761803916770790967 ),
 .UNSPECIFIED. ) ;
#30344=EDGE_LOOP ( 'NONE', ( #286, #89664, #34830, #6417 ) ) ;
#30346=ORIENTED_EDGE ( 'NONE', *, *, #54713, .T. ) ;
#30348=CARTESIAN_POINT ( 'NONE',  ( -80.51244414166535535, -29.50249942614373921, 7.563164501610022405 ) ) ;
#30351=CARTESIAN_POINT ( 'NONE',  ( -55.52287095715004739, -24.51254535375842991, 9.355368624242258235 ) ) ;
#30352=CARTESIAN_POINT ( 'NONE',  ( -65.54557472772603433, -24.40034930558991277, 0.3402023900116039612 ) ) ;
#30353=CARTESIAN_POINT ( 'NONE',  ( -20.58003014649542095, 7.718188279156099618, 11.49999999999999645 ) ) ;
#30355=CARTESIAN_POINT ( 'NONE',  ( 1.525329354412473970, -22.51392980886878448, -1.500000000000002220 ) ) ;
#30357=CARTESIAN_POINT ( 'NONE',  ( 5.724939850241691275, 20.19279902153374096, 11.49999999999998934 ) ) ;
#30365=CARTESIAN_POINT ( 'NONE',  ( -2.374466145016132845, -21.38244973876172494, -1.500000000000002220 ) ) ;
#30368=PLANE ( 'NONE',  #68345 ) ;
#30369=VERTEX_POINT ( 'NONE', #59734 ) ;
#30370=CARTESIAN_POINT ( 'NONE',  ( 0.3207198112191017025, -21.10926996749724083, -1.500000000000002220 ) ) ;
#30371=FACE_OUTER_BOUND ( 'NONE', #40554, .T. ) ;
#30372=CARTESIAN_POINT ( 'NONE',  ( -64.49992615054290468, -24.34968618360933235, 0.1864209137778785330 ) ) ;
#30373=CARTESIAN_POINT ( 'NONE',  ( -83.62924211730506840, -24.35071581493543036, 9.817618358456028815 ) ) ;
#30374=CARTESIAN_POINT ( 'NONE',  ( -104.6228709571500559, -24.64898659630529210, 1.056161002820829697 ) ) ;
#30375=CARTESIAN_POINT ( 'NONE',  ( -69.94583786925741720, -25.25893427375708455, 3.680069841752215964 ) ) ;
#30376=CARTESIAN_POINT ( 'NONE',  ( 22.09269804725545683, -1.632937629565654580, -1.500000000000002220 ) ) ;
#30377=CARTESIAN_POINT ( 'NONE',  ( -71.63963700100102017, -23.96119346886880308, -0.6495511937832095795 ) ) ;
#30378=B_SPLINE_CURVE_WITH_KNOTS ( 'NONE', 3,
 ( #47234, #71078, #23368, #24884 ),
 .UNSPECIFIED., .F., .F.,
 ( 4, 4 ),
 ( 0.000000000000000000, 0.0001000000000000028644 ),
 .UNSPECIFIED. ) ;
#30380=CARTESIAN_POINT ( 'NONE',  ( -51.35838135674943317, -25.24860032974256541, 5.126937756223604481 ) ) ;
#30381=CARTESIAN_POINT ( 'NONE',  ( -67.58953762381672448, -24.64898659630367916, 1.056161002820384054 ) ) ;
#30383=B_SPLINE_CURVE_WITH_KNOTS ( 'NONE', 3,
 ( #62063, #55450, #70667, #8770, #86886, #39205, #87387, #64084 ),
 .UNSPECIFIED., .F., .F.,
 ( 4, 2, 2, 4 ),
 ( -0.001240355328176889803, -0.0002398155169399719417, 0.0007607242942969459198, 0.002761803916770781860 ),
 .UNSPECIFIED. ) ;
#30384=CARTESIAN_POINT ( 'NONE',  ( -64.62287095715005592, -24.64965695001468404, 8.947790433994185832 ) ) ;
#30385=CARTESIAN_POINT ( 'NONE',  ( -15.63568348323273227, -11.59263941501104966, -1.500000000000002220 ) ) ;
#30386=CARTESIAN_POINT ( 'NONE',  ( -1.242826169824672977, 21.35102975155811222, -1.500000000000002220 ) ) ;
#30388=CARTESIAN_POINT ( 'NONE',  ( -42.52287095715005449, -29.50250786944525672, 11.44777988621624232 ) ) ;
#30389=CARTESIAN_POINT ( 'NONE',  ( -72.52287095715007581, -23.47596703998600631, 11.44779298504228748 ) ) ;
#30390=LINE ( 'NONE', #20767, #63626 ) ;
#30391=CARTESIAN_POINT ( 'NONE',  ( -21.51096707683950626, -7.176001652309477841, -1.500000000000002220 ) ) ;
#30394=PLANE ( 'NONE',  #47609 ) ;
#30395=CARTESIAN_POINT ( 'NONE',  ( 14.45944668481935658, 13.51102189132778442, 11.49999999999999645 ) ) ;
#30398=DIRECTION ( 'NONE',  ( 0.000000000000000000, -0.9999999999976377785, -2.173523156925979128E-06 ) ) ;
#30399=ORIENTED_EDGE ( 'NONE', *, *, #45124, .T. ) ;
#30400=CARTESIAN_POINT ( 'NONE',  ( -66.58953762381672448, -24.64898659630367916, 1.056161002820382722 ) ) ;
#30401=CARTESIAN_POINT ( 'NONE',  ( -61.64687923781919920, -25.14083923594766645, 2.947789366383931853 ) ) ;
#30403=CARTESIAN_POINT ( 'NONE',  ( 21.43499300031224664, 3.042053824063517542, 11.49999999999998934 ) ) ;
#30404=AXIS2_PLACEMENT_3D ( 'NONE', #98492, #99980, #28994 ) ;
#30405=EDGE_CURVE ( 'NONE', #63299, #23903, #25301, .T. ) ;
#30406=LINE ( 'NONE', #69971, #88539 ) ;
#30407=CARTESIAN_POINT ( 'NONE',  ( 17.65527434030279252, -8.155491144718855168, -1.500000000000002220 ) ) ;
#30409=CARTESIAN_POINT ( 'NONE',  ( -82.52287095715011844, -24.51387760970725083, 9.387446482453416507 ) ) ;
#30411=CARTESIAN_POINT ( 'NONE',  ( 16.01007288495529224, -11.65062672332236104, 11.49999999999998934 ) ) ;
#30412=EDGE_LOOP ( 'NONE', ( #31617, #6805, #78633, #74635 ) ) ;
#30413=EDGE_CURVE ( 'NONE', #47659, #56669, #99752, .T. ) ;
#30414=CARTESIAN_POINT ( 'NONE',  ( 3.964343641299885146, 19.94596313931659992, 11.49999999999999645 ) ) ;
#30415=CARTESIAN_POINT ( 'NONE',  ( -80.64599942773482155, -23.85016227208580020, -0.8807180028928338622 ) ) ;
#30417=ORIENTED_EDGE ( 'NONE', *, *, #54162, .T. ) ;
#30418=CARTESIAN_POINT ( 'NONE',  ( -30.56688274934923299, -25.56688301298833821, 3.825958421598585790 ) ) ;
#30419=DIRECTION ( 'NONE',  ( -3.773278334444167608E-23, 1.000000000000000000, 0.000000000000000000 ) ) ;
#30421=B_SPLINE_CURVE_WITH_KNOTS ( 'NONE', 3,
 ( #41802, #64148, #87963, #48910, #40783, #26568, #10333, #49415 ),
 .UNSPECIFIED., .F., .F.,
 ( 4, 2, 2, 4 ),
 ( -0.001240666984355828697, -0.0002401179793394868714, 0.0007604310256768549540, 0.002761529035709537738 ),
 .UNSPECIFIED. ) ;
#30422=CARTESIAN_POINT ( 'NONE',  ( -40.66403789857419326, -23.85049219812685095, 10.88485053497527488 ) ) ;
#30423=CARTESIAN_POINT ( 'NONE',  ( -127.6228709571500275, -24.33927499327854704, 9.819080762295811837 ) ) ;
#30424=CARTESIAN_POINT ( 'NONE',  ( -19.29710791919172053, 5.528754708966634901, -1.500000000000002220 ) ) ;
#30425=EDGE_CURVE ( 'NONE', #71428, #11978, #92155, .T. ) ;
#30426=EDGE_CURVE ( 'NONE', #89034, #47332, #58031, .T. ) ;
#30431=CARTESIAN_POINT ( 'NONE',  ( -21.29394331855728240, -8.360804490491451801, 11.49999999999999645 ) ) ;
#30432=CARTESIAN_POINT ( 'NONE',  ( -19.63924127562733446, 11.44998032699685631, -1.500000000000002220 ) ) ;
#30433=CARTESIAN_POINT ( 'NONE',  ( -49.50986403386431078, -25.26258728624853234, 4.014908451308841109 ) ) ;
#30437=B_SPLINE_CURVE_WITH_KNOTS ( 'NONE', 3,
 ( #26256, #80039, #88160, #10024, #17639, #9525, #10525, #57228, #18139, #18630 ),
 .UNSPECIFIED., .F., .F.,
 ( 4, 2, 2, 2, 4 ),
 ( 0.000000000000000000, 0.0002557780953295595299, 0.0005115561906591190597, 0.0007673342859886786438, 0.001023112381318238119 ),
 .UNSPECIFIED. ) ;
#30442=LINE ( 'NONE', #46678, #90628 ) ;
#30445=CARTESIAN_POINT ( 'NONE',  ( 17.42226438573850800, -10.51879874471254261, -1.500000000000002220 ) ) ;
#30446=ORIENTED_EDGE ( 'NONE', *, *, #47245, .F. ) ;
#30447=CARTESIAN_POINT ( 'NONE',  ( -2.116611060711651504, 22.89395876494169002, -1.500000000000002220 ) ) ;
#30450=VERTEX_POINT ( 'NONE', #32261 ) ;
#30452=EDGE_CURVE ( 'NONE', #28633, #44325, #55112, .T. ) ;
#30453=CARTESIAN_POINT ( 'NONE',  ( -77.63799604921862851, -23.96169478059713498, 10.65365249895717703 ) ) ;
#30455=CARTESIAN_POINT ( 'NONE',  ( -51.62368732844929298, -24.66019654487199730, 8.947790411086117501 ) ) ;
#30456=CARTESIAN_POINT ( 'NONE',  ( -13.45305159987462851, 16.49040971879131234, 11.49999999999999645 ) ) ;
#30457=VERTEX_POINT ( 'NONE', #8427 ) ;
#30459=CARTESIAN_POINT ( 'NONE',  ( -5.848988146064017180, 21.40304369876291446, -1.500000000000002220 ) ) ;
#30460=CARTESIAN_POINT ( 'NONE',  ( -7.658335995763069448, 19.15843701367676388, -1.500000000000002220 ) ) ;
#30461=ORIENTED_EDGE ( 'NONE', *, *, #74187, .F. ) ;
#30463=CARTESIAN_POINT ( 'NONE',  ( -109.5136315545911856, -25.31627384547671511, 5.394825593643450823 ) ) ;
#30465=CARTESIAN_POINT ( 'NONE',  ( -39.05141833839561372, -25.27719696402067129, 4.032623266159655273 ) ) ;
#30466=ORIENTED_EDGE ( 'NONE', *, *, #53805, .T. ) ;
#30467=CARTESIAN_POINT ( 'NONE',  ( -49.34124502834663417, -25.22564238971922990, 6.480461498194810765 ) ) ;
#30468=ORIENTED_EDGE ( 'NONE', *, *, #5463, .T. ) ;
#30470=DIRECTION ( 'NONE',  ( -3.773278334453079618E-23, 0.9999999999976377785, 2.173523156925979975E-06 ) ) ;
#30471=CARTESIAN_POINT ( 'NONE',  ( 1.081820405348005165, -20.78239343107542680, -1.500000000000002220 ) ) ;
#30472=CARTESIAN_POINT ( 'NONE',  ( 14.98227958311676744, 15.82868232077399462, 11.49999999999999645 ) ) ;
#30473=CARTESIAN_POINT ( 'NONE',  ( -90.52380231474228367, -25.22391154813774250, 6.409327647370975711 ) ) ;
#30474=CARTESIAN_POINT ( 'NONE',  ( -100.2506239054133204, -25.03433485709489759, 7.556303271660354426 ) ) ;
#30475=CARTESIAN_POINT ( 'NONE',  ( 22.31695869535024102, -2.478243017838637652, 11.49999999999998934 ) ) ;
#30476=CARTESIAN_POINT ( 'NONE',  ( -51.29424904866267099, -25.31296618838156931, 4.063411898103660214 ) ) ;
#30478=DIRECTION ( 'NONE',  ( -0.000000000000000000, 2.173523156925979552E-06, -0.9999999999976378895 ) ) ;
#30479=CARTESIAN_POINT ( 'NONE',  ( -50.46342637979365264, -25.11078852230776803, 2.834907798866269868 ) ) ;
#30480=B_SPLINE_SURFACE_WITH_KNOTS ( 'NONE', 3, 1, ( 
 ( #51507, #29153 ),
 ( #51010, #37766 ),
 ( #43398, #68723 ),
 ( #98654, #60126 ),
 ( #30143, #98153 ),
 ( #68225, #52502 ),
 ( #97668, #91547 ),
 ( #99152, #21525 ),
 ( #20533, #83432 ),
 ( #81944, #13920 ),
 ( #29652, #14419 ),
 ( #44897, #59621 ),
 ( #60626, #53009 ),
 ( #22020, #90554 ),
 ( #12430, #82439 ),
 ( #75322, #83939 ),
 ( #91052, #5317 ),
 ( #45394, #28660 ),
 ( #28166, #75819 ) ),
 .UNSPECIFIED., .F., .F., .F.,
 ( 4, 1, 1, 1, 1, 1, 1, 1, 1, 1, 1, 1, 1, 1, 1, 1, 4 ),
 ( 2, 2 ),
 ( 0.000000000000000000, 0.05527454908752621465, 0.1099660938819831402, 0.1632474428518071730, 0.2180761854823636270, 0.2733008743735952928, 0.3309093000114374239, 0.3909945233652084573, 0.4541759534308271173, 0.5188615408488264080, 0.5833105320111698910, 0.6485166818638251618, 0.7150308870971843200, 0.7825020728543330417, 0.8523226850768604868, 0.9249284897844326503, 1.000000000000000000 ),
 ( 0.000000000000000000, 1.000000000000000000 ),
 .UNSPECIFIED. ) ;
#30482=VERTEX_POINT ( 'NONE', #86549 ) ;
#30483=ORIENTED_EDGE ( 'NONE', *, *, #6797, .T. ) ;
#30484=CARTESIAN_POINT ( 'NONE',  ( -19.99122433398336440, 7.574256484821010105, -1.500000000000002220 ) ) ;
#30486=CARTESIAN_POINT ( 'NONE',  ( 8.881738082190086203, 19.07353979602852689, 11.49999999999998934 ) ) ;
#30487=CARTESIAN_POINT ( 'NONE',  ( -30.60464189315247907, -24.58218713401908317, 0.8299800598022480935 ) ) ;
#30488=CARTESIAN_POINT ( 'NONE',  ( -41.46355252140796210, -25.28892596830917228, 4.097884790672636335 ) ) ;
#30489=DIRECTION ( 'NONE',  ( -3.773278334453079618E-23, 0.9999999999976377785, 2.173523156925979975E-06 ) ) ;
#30490=CARTESIAN_POINT ( 'NONE',  ( 8.537626919312410578, 20.26776412955123163, -1.500000000000002220 ) ) ;
#30491=CARTESIAN_POINT ( 'NONE',  ( -87.58840615572438537, -24.34968618360935011, 0.1864209137778971292 ) ) ;
#30493=CARTESIAN_POINT ( 'NONE',  ( -83.62287095715005592, -29.50250786944525672, 11.44777988621623521 ) ) ;
#30497=CARTESIAN_POINT ( 'NONE',  ( -33.62287095715005592, -23.48783264082477373, -1.443836473390074371 ) ) ;
#30498=CARTESIAN_POINT ( 'NONE',  ( -30.62049582358472222, -24.26855077790994386, 9.960784317162937995 ) ) ;
#30499=CARTESIAN_POINT ( 'NONE',  ( 12.11089201280794470, -17.53110042540249225, -1.500000000000002220 ) ) ;
#30500=CARTESIAN_POINT ( 'NONE',  ( -98.62981689697267029, -24.15620529776628800, 10.23563542870660292 ) ) ;
#30501=CARTESIAN_POINT ( 'NONE',  ( -27.68651082257923335, -24.75185970166884175, 2.274903409718059599 ) ) ;
#30504=CARTESIAN_POINT ( 'NONE',  ( -70.52287095715007581, -24.91544648472625667, 1.928969306349430868 ) ) ;
#30505=CARTESIAN_POINT ( 'NONE',  ( 22.08653571170524543, -4.319401766784854324, -1.500000000000002220 ) ) ;
#30506=ADVANCED_FACE ( 'NONE', ( #70331, #47497, #100246, #93148, #69326, #54120, #70834, #48001, #9420, #85043, #15529, #86048 ), #55531, .T. ) ;
#30507=CARTESIAN_POINT ( 'NONE',  ( -110.9396397263220990, -25.30561928443788133, 5.929683345795315752 ) ) ;
#30508=ORIENTED_EDGE ( 'NONE', *, *, #82207, .T. ) ;
#30509=EDGE_CURVE ( 'NONE', #4409, #55534, #16845, .T. ) ;
#30510=CARTESIAN_POINT ( 'NONE',  ( -99.28737118923764626, -25.13419999133549965, 7.096671994546412066 ) ) ;
#30511=CARTESIAN_POINT ( 'NONE',  ( 18.70796670040472165, 5.986831462552164140, 11.49999999999999645 ) ) ;
#30512=CARTESIAN_POINT ( 'NONE',  ( -128.6228709571500417, -23.48783264082479505, -1.443836473390056829 ) ) ;
#30517=EDGE_CURVE ( 'NONE', #1418, #60061, #12420, .T. ) ;
#30518=CARTESIAN_POINT ( 'NONE',  ( -50.55620429048337883, -23.48783264082477729, -1.443836473390070152 ) ) ;
#30519=CARTESIAN_POINT ( 'NONE',  ( -42.62287095715004881, -24.64965695001467694, 8.947790433994187609 ) ) ;
#30520=CARTESIAN_POINT ( 'NONE',  ( -100.6814946224345846, -25.31439533081184479, 5.197788989161054474 ) ) ;
#30521=ADVANCED_FACE ( 'NONE', ( #37265 ), #74328, .T. ) ;
#30523=CARTESIAN_POINT ( 'NONE',  ( -19.47062899137607772, 3.135797168518691169, -1.500000000000002220 ) ) ;
#30524=ORIENTED_EDGE ( 'NONE', *, *, #25289, .F. ) ;
#30526=CARTESIAN_POINT ( 'NONE',  ( -120.5228709571500616, -23.48786465467241769, 11.44779295918253759 ) ) ;
#30527=CARTESIAN_POINT ( 'NONE',  ( -118.5228709571501042, -24.51283580621365488, 0.6167428607019833642 ) ) ;
#30529=EDGE_LOOP ( 'NONE', ( #2036, #58551, #25089, #40873 ) ) ;
#30531=LINE ( 'NONE', #100017, #45829 ) ;
#30533=CARTESIAN_POINT ( 'NONE',  ( -99.09546795806416242, -25.26638384523103653, 6.840687619165027655 ) ) ;
#30535=LINE ( 'NONE', #93935, #10056 ) ;
#30537=CARTESIAN_POINT ( 'NONE',  ( 19.63333621495807435, 3.783328549194958867, -1.500000000000002220 ) ) ;
#30538=EDGE_CURVE ( 'NONE', #52671, #13507, #21515, .T. ) ;
#30539=CARTESIAN_POINT ( 'NONE',  ( -100.2631815169052203, -25.10935038814901787, 2.837686026794785210 ) ) ;
#30541=ORIENTED_EDGE ( 'NONE', *, *, #5495, .F. ) ;
#30542=EDGE_CURVE ( 'NONE', #43961, #28152, #32670, .T. ) ;
#30543=CARTESIAN_POINT ( 'NONE',  ( -119.5576576810219507, -23.48783264082477373, -1.443836473390087916 ) ) ;
#30544=CARTESIAN_POINT ( 'NONE',  ( -80.60234139019381416, -23.85049219812686161, 10.88485053497527311 ) ) ;
#30548=CARTESIAN_POINT ( 'NONE',  ( -45.55620429048339304, -25.00182538069144655, 7.747789668545097541 ) ) ;
#30549=B_SPLINE_SURFACE_WITH_KNOTS ( 'NONE', 3, 3, ( 
 ( #71136, #48810, #8733, #39670 ),
 ( #25453, #95969, #56428, #71636 ),
 ( #3139, #2138, #79735, #26468 ),
 ( #18347, #32060, #17849, #72145 ),
 ( #63035, #1630, #10231, #2632 ),
 ( #25956, #87859, #86843, #64050 ),
 ( #93956, #34080, #80244, #24447 ) ),
 .UNSPECIFIED., .F., .F., .F.,
 ( 4, 3, 4 ),
 ( 4, 4 ),
 ( 0.7945040050992248082, 0.8970133687736506767, 0.9995227324480765452 ),
 ( 0.7096743353268654131, 0.7110146926484223195 ),
 .UNSPECIFIED. ) ;
#30551=CARTESIAN_POINT ( 'NONE',  ( -40.52287095715006870, -24.14406661686763300, 10.28769366194071466 ) ) ;
#30553=CARTESIAN_POINT ( 'NONE',  ( -16.53579703214142427, -11.71821515807347680, -1.500000000000002220 ) ) ;
#30554=CARTESIAN_POINT ( 'NONE',  ( -122.5889747868830284, -24.51314013834316086, 0.6176544820404212821 ) ) ;
#30555=B_SPLINE_CURVE_WITH_KNOTS ( 'NONE', 3,
 ( #43555, #88735, #64920, #95835 ),
 .UNSPECIFIED., .F., .F.,
 ( 4, 4 ),
 ( 0.9404574821454589895, 0.9494639134175745232 ),
 .UNSPECIFIED. ) ;
#30556=CARTESIAN_POINT ( 'NONE',  ( -33.62287095715005592, -29.50250243563736774, 8.947779886222150481 ) ) ;
#30557=VECTOR ( 'NONE', #6335, 1000.000000000000114 ) ;
#30558=B_SPLINE_CURVE_WITH_KNOTS ( 'NONE', 3,
 ( #46962, #77883, #8389, #39337, #70298, #779 ),
 .UNSPECIFIED., .F., .F.,
 ( 4, 2, 4 ),
 ( 0.000000000000000000, 0.001380901958385388545, 0.002761803916770777089 ),
 .UNSPECIFIED. ) ;
#30559=CARTESIAN_POINT ( 'NONE',  ( -40.94687764114259920, -25.04307374350000259, 7.563175304812659761 ) ) ;
#30560=ADVANCED_FACE ( 'NONE', ( #59611 ), #36269, .T. ) ;
#30561=EDGE_LOOP ( 'NONE', ( #78569, #26520, #26837, #25460 ) ) ;
#30562=PLANE ( 'NONE',  #1603 ) ;
#30563=CARTESIAN_POINT ( 'NONE',  ( -9.210493908506615313, -17.87979239004878451, -1.500000000000002220 ) ) ;
#30564=CARTESIAN_POINT ( 'NONE',  ( -20.42954818520503935, 5.180689535515515587, 11.49999999999999645 ) ) ;
#30565=CARTESIAN_POINT ( 'NONE',  ( -32.58953762381672448, -24.65952944569304606, 1.056160979905698571 ) ) ;
#30566=CARTESIAN_POINT ( 'NONE',  ( -13.28819421967561532, -17.68372732473523001, -1.500000000000002220 ) ) ;
#30568=CARTESIAN_POINT ( 'NONE',  ( 17.96566822227200433, 9.963707542159163211, -1.500000000000002220 ) ) ;
#30569=CARTESIAN_POINT ( 'NONE',  ( -70.52287095715007581, -29.50248789122583659, 2.256150453626215580 ) ) ;
#30570=CARTESIAN_POINT ( 'NONE',  ( -60.64004623127358684, -24.40034930558990922, 0.3402023900116026289 ) ) ;
#30571=ORIENTED_EDGE ( 'NONE', *, *, #18792, .T. ) ;
#30575=DIRECTION ( 'NONE',  ( -3.773278334453079618E-23, 0.9999999999976377785, 2.173523156925979975E-06 ) ) ;
#30576=ORIENTED_EDGE ( 'NONE', *, *, #28294, .T. ) ;
#30581=CARTESIAN_POINT ( 'NONE',  ( -49.25194410911545617, -25.12154037719012933, 7.110284505066584160 ) ) ;
#30583=CARTESIAN_POINT ( 'NONE',  ( 3.034461355793923509, -20.43525710956717845, -1.500000000000002220 ) ) ;
#30584=CARTESIAN_POINT ( 'NONE',  ( 9.069627533930374241, 19.64968329815391712, 11.49999999999999645 ) ) ;
#30585=ORIENTED_EDGE ( 'NONE', *, *, #95286, .T. ) ;
#30588=CARTESIAN_POINT ( 'NONE',  ( -21.65924713590726469, 5.634197536097032888, -1.500000000000002220 ) ) ;
#30589=DIRECTION ( 'NONE',  ( 0.000000000000000000, -2.173523156925979552E-06, 0.9999999999976378895 ) ) ;
#30590=CARTESIAN_POINT ( 'NONE',  ( -82.62287095715005592, -23.47593901973091235, -1.443836447539004642 ) ) ;
#30591=ORIENTED_EDGE ( 'NONE', *, *, #90840, .T. ) ;
#30594=CARTESIAN_POINT ( 'NONE',  ( -115.5228709571500332, -24.51163499207174823, 0.6490370598554319193 ) ) ;
#30595=CARTESIAN_POINT ( 'NONE',  ( -16.12721948686093754, -13.32240427740599564, -1.500000000000002220 ) ) ;
#30596=ORIENTED_EDGE ( 'NONE', *, *, #64232, .F. ) ;
#30597=CARTESIAN_POINT ( 'NONE',  ( -86.58308328051593605, -24.65952944569304606, 1.056160979905700126 ) ) ;
#30598=EDGE_LOOP ( 'NONE', ( #32336, #25890, #86918, #75991 ) ) ;
#30599=VECTOR ( 'NONE', #67245, 1000.000000000000114 ) ;
#30600=CARTESIAN_POINT ( 'NONE',  ( -50.62287095715005592, -24.99156045073392463, 7.747789690856161648 ) ) ;
#30601=CARTESIAN_POINT ( 'NONE',  ( 18.56724428474754518, 10.22298014144217859, -1.500000000000002220 ) ) ;
#30602=ORIENTED_EDGE ( 'NONE', *, *, #93173, .F. ) ;
#30603=CARTESIAN_POINT ( 'NONE',  ( -117.6270223626581384, -23.96119346886881019, -0.6495511937831995875 ) ) ;
#30604=CARTESIAN_POINT ( 'NONE',  ( -99.87501341000351829, -25.26221294576034637, 6.992709272975608847 ) ) ;
#30605=CARTESIAN_POINT ( 'NONE',  ( 21.06710269851327766, -5.618397932909799941, -1.500000000000002220 ) ) ;
#30606=FACE_OUTER_BOUND ( 'NONE', #43176, .T. ) ;
#30607=DIRECTION ( 'NONE',  ( -3.773278334444167608E-23, 1.000000000000000000, 0.000000000000000000 ) ) ;
#30608=CARTESIAN_POINT ( 'NONE',  ( -84.62287095715005592, -24.64965695001469115, 8.947790433994182280 ) ) ;
#30609=CARTESIAN_POINT ( 'NONE',  ( -15.04333773895388937, -15.80532200100455498, -1.500000000000002220 ) ) ;
#30610=CARTESIAN_POINT ( 'NONE',  ( -41.55620429048340014, -24.64898659630529210, 1.056161002820823036 ) ) ;
#30615=ORIENTED_EDGE ( 'NONE', *, *, #42697, .F. ) ;
#30616=ORIENTED_EDGE ( 'NONE', *, *, #59401, .T. ) ;
#30618=CARTESIAN_POINT ( 'NONE',  ( -125.9228709571500531, -23.47596703998600631, 11.44779298504227860 ) ) ;
#30619=CARTESIAN_POINT ( 'NONE',  ( 3.302162439418223627, -20.95225242093645690, -1.500000000000002220 ) ) ;
#30620=CARTESIAN_POINT ( 'NONE',  ( -119.6228709571500559, -24.64965695001469115, 8.947790433994175174 ) ) ;
#30621=CARTESIAN_POINT ( 'NONE',  ( -79.02216967728209340, -25.03138069755155470, 6.505901493516774714 ) ) ;
#30622=B_SPLINE_CURVE_WITH_KNOTS ( 'NONE', 3,
 ( #63474, #69567, #45, #99963, #94371, #46200 ),
 .UNSPECIFIED., .F., .F.,
 ( 4, 2, 4 ),
 ( 0.000000000000000000, 0.001380764517853247516, 0.002761529035706495033 ),
 .UNSPECIFIED. ) ;
#30623=DIRECTION ( 'NONE',  ( 0.000000000000000000, -2.173523156925979552E-06, 0.9999999999976378895 ) ) ;
#30625=CARTESIAN_POINT ( 'NONE',  ( -17.02366064725396555, -9.230830265533395362, 11.49999999999998934 ) ) ;
#30627=CARTESIAN_POINT ( 'NONE',  ( -69.48331070941586063, -25.29418496701295282, 5.732640622402496611 ) ) ;
#30630=EDGE_CURVE ( 'NONE', #96177, #70011, #13251, .T. ) ;
#30631=CARTESIAN_POINT ( 'NONE',  ( -19.46337940159461866, -0.4807646128305608779, 11.49999999999999645 ) ) ;
#30632=CARTESIAN_POINT ( 'NONE',  ( -107.6228709571500701, -23.47596703998600631, 11.44779298504227860 ) ) ;
#30634=CARTESIAN_POINT ( 'NONE',  ( -49.62287095715007013, -24.50321055353804667, 9.387540953477540029 ) ) ;
#30635=ORIENTED_EDGE ( 'NONE', *, *, #58853, .T. ) ;
#30636=EDGE_CURVE ( 'NONE', #96384, #11381, #21024, .T. ) ;
#30640=EDGE_CURVE ( 'NONE', #3242, #76617, #71324, .T. ) ;
#30641=DIRECTION ( 'NONE',  ( 0.000000000000000000, -0.9999999999976377785, -2.173523156925979975E-06 ) ) ;
#30642=CARTESIAN_POINT ( 'NONE',  ( -55.62287095715004881, -23.85196035786900026, -0.8779234886474988064 ) ) ;
#30643=CARTESIAN_POINT ( 'NONE',  ( -8.122062702759739850, 17.86989387945112995, -1.500000000000002220 ) ) ;
#30644=EDGE_CURVE ( 'NONE', #12095, #9929, #66495, .T. ) ;
#30645=CARTESIAN_POINT ( 'NONE',  ( -41.42418673051398770, -25.31583634048925902, 4.451103923698910947 ) ) ;
#30647=CARTESIAN_POINT ( 'NONE',  ( 10.40854797073303395, 18.91789161722374146, -1.500000000000002220 ) ) ;
#30649=B_SPLINE_CURVE_WITH_KNOTS ( 'NONE', 3,
 ( #8751, #55939, #48828, #39689, #40200, #70648, #32078, #1646, #16856, #10247, #32581, #41209, #63561, #72162, #66065, #43701, #89870, #88377 ),
 .UNSPECIFIED., .F., .F.,
 ( 4, 2, 2, 2, 2, 2, 2, 2, 4 ),
 ( 0.000000000000000000, 0.0002916214222385914677, 0.0005832428444771829354, 0.0008748642667157744031, 0.001166485688954365871, 0.001458107111192957338, 0.001749728533431548806, 0.002041349955670140274, 0.002332971377908731742 ),
 .UNSPECIFIED. ) ;
#30654=CARTESIAN_POINT ( 'NONE',  ( -20.90396053131702914, -9.656267258341529214, -1.500000000000002220 ) ) ;
#30656=CARTESIAN_POINT ( 'NONE',  ( -127.5228709571500616, -23.47593901973090524, -1.443836447538996204 ) ) ;
#30658=CARTESIAN_POINT ( 'NONE',  ( 18.63370447891095694, 7.782165041754079304, 11.49999999999999645 ) ) ;
#30660=CARTESIAN_POINT ( 'NONE',  ( -101.7482071278742808, -25.17643464477231063, 6.839252989080933709 ) ) ;
#30662=CARTESIAN_POINT ( 'NONE',  ( -57.62287095715004881, -24.64965695001468404, 8.947790433994185832 ) ) ;
#30663=CARTESIAN_POINT ( 'NONE',  ( -129.6238141773120560, -23.73766607897671577, -1.055555164236443577 ) ) ;
#30664=CARTESIAN_POINT ( 'NONE',  ( -111.3663525145439053, -25.18425782680516178, 4.214194604219601459 ) ) ;
#30665=CARTESIAN_POINT ( 'NONE',  ( 4.300141163375406528, 19.41444791797076874, 11.49999999999998934 ) ) ;
#30666=CARTESIAN_POINT ( 'NONE',  ( -118.5228709571500758, -23.48786465467241769, 11.44779295918253759 ) ) ;
#30667=CARTESIAN_POINT ( 'NONE',  ( 14.04693994163893578, -13.95676237773968609, -1.500000000000002220 ) ) ;
#30668=CARTESIAN_POINT ( 'NONE',  ( -56.49251241998729256, -24.51314013834315730, 0.6176544820404098468 ) ) ;
#30669=CARTESIAN_POINT ( 'NONE',  ( -39.57984969116796492, -25.10925652639403793, 3.109569470329076157 ) ) ;
#30671=CARTESIAN_POINT ( 'NONE',  ( 10.87737074370964407, 17.65887017642603851, 11.49999999999999645 ) ) ;
#30672=CARTESIAN_POINT ( 'NONE',  ( -53.52287095715005449, -24.66019654487198665, 8.947790411086121054 ) ) ;
#30673=CARTESIAN_POINT ( 'NONE',  ( -50.34100630499489881, -25.31439277421117851, 5.198616746494224117 ) ) ;
#30674=VECTOR ( 'NONE', #100137, 1000.000000000000114 ) ;
#30675=CARTESIAN_POINT ( 'NONE',  ( 21.55457256799317278, 7.124301260279622738, 11.49999999999999645 ) ) ;
#30676=VERTEX_POINT ( 'NONE', #61615 ) ;
#30679=CARTESIAN_POINT ( 'NONE',  ( 19.60372117168125072, 4.849774137724135237, 11.49999999999998934 ) ) ;
#30681=CARTESIAN_POINT ( 'NONE',  ( -52.58953762381671737, -23.47593901973091235, -1.443836447539009749 ) ) ;
#30682=VERTEX_POINT ( 'NONE', #85422 ) ;
#30683=ORIENTED_EDGE ( 'NONE', *, *, #83123, .F. ) ;
#30685=CARTESIAN_POINT ( 'NONE',  ( 22.67525425759127344, 3.225002893152739247, -1.500000000000002220 ) ) ;
#30686=CARTESIAN_POINT ( 'NONE',  ( -50.97853604095990221, -25.27420597387646595, 3.451784371543335617 ) ) ;
#30687=B_SPLINE_CURVE_WITH_KNOTS ( 'NONE', 3,
 ( #46482, #34760, #2822, #9915, #94652, #49499 ),
 .UNSPECIFIED., .F., .F.,
 ( 4, 2, 4 ),
 ( 1.570887131794952276E-05, 0.001396322306279766711, 0.002776935741241583645 ),
 .UNSPECIFIED. ) ;
#30688=CARTESIAN_POINT ( 'NONE',  ( -7.466173891270859286, -20.28576548065916541, -1.500000000000002220 ) ) ;
#30689=DIRECTION ( 'NONE',  ( 1.000000000000000000, 3.773278334444167608E-23, 8.201307833595939069E-29 ) ) ;
#30690=CARTESIAN_POINT ( 'NONE',  ( -34.57049221944907913, -23.48783264082478084, -1.443836473390076591 ) ) ;
#30691=CARTESIAN_POINT ( 'NONE',  ( 12.70736309587848645, -16.60074808024427284, 11.49999999999999645 ) ) ;
#30692=ORIENTED_EDGE ( 'NONE', *, *, #68333, .F. ) ;
#30693=CARTESIAN_POINT ( 'NONE',  ( -124.6261987484861748, -23.48783264082478084, -1.443836473390086361 ) ) ;
#30694=CARTESIAN_POINT ( 'NONE',  ( -20.87105610827876134, -7.033761084331515256, 11.49999999999998934 ) ) ;
#30696=MANIFOLD_SURFACE_SHAPE_REPRESENTATION ( '', ( #29565, #218 ), #69909 ) ;
#30697=CARTESIAN_POINT ( 'NONE',  ( -105.5519745381963190, -24.40133493613049964, 9.663955038902797057 ) ) ;
#30700=CARTESIAN_POINT ( 'NONE',  ( -73.62287095715005592, -23.47593901973091235, -1.443836447539006196 ) ) ;
#30702=CARTESIAN_POINT ( 'NONE',  ( -46.55620429048338593, -23.48783264082477729, -1.443836473390070596 ) ) ;
#30703=EDGE_LOOP ( 'NONE', ( #64128, #88280, #35272, #10998, #24083, #45214, #66184, #34576, #59324, #8284, #69894, #40700, #59051, #57826 ) ) ;
#30704=CARTESIAN_POINT ( 'NONE',  ( -72.63936762441933581, -23.96169478059713143, 10.65365249895718414 ) ) ;
#30706=VECTOR ( 'NONE', #79873, 1000.000000000000114 ) ;
#30707=ORIENTED_EDGE ( 'NONE', *, *, #59638, .T. ) ;
#30711=CARTESIAN_POINT ( 'NONE',  ( 19.83930831332124001, -5.160774681608516268, -1.500000000000002220 ) ) ;
#30717=CARTESIAN_POINT ( 'NONE',  ( -5.617636847906702258, 21.56867655435222630, -1.500000000000002220 ) ) ;
#30718=PLANE ( 'NONE',  #2750 ) ;
#30719=CARTESIAN_POINT ( 'NONE',  ( -47.62287095715004881, -23.48786465467240703, 11.44779295918255180 ) ) ;
#30720=ORIENTED_EDGE ( 'NONE', *, *, #58212, .T. ) ;
#30721=CARTESIAN_POINT ( 'NONE',  ( -28.43450822049934956, -24.70030246006994901, 1.766382807631876606 ) ) ;
#30722=AXIS2_PLACEMENT_3D ( 'NONE', #14210, #69010, #74618 ) ;
#30723=CARTESIAN_POINT ( 'NONE',  ( -29.12273499046074221, -24.63645922367957297, 7.596952268176241141 ) ) ;
#30725=CARTESIAN_POINT ( 'NONE',  ( -17.17656601037699104, 11.78060583124977256, -1.500000000000002220 ) ) ;
#30726=ORIENTED_EDGE ( 'NONE', *, *, #96905, .T. ) ;
#30727=FACE_OUTER_BOUND ( 'NONE', #39712, .T. ) ;
#30728=EDGE_LOOP ( 'NONE', ( #7346, #33336, #60691, #15948 ) ) ;
#30730=CARTESIAN_POINT ( 'NONE',  ( -51.52241826985714113, -25.25854396960094661, 6.308158736584201343 ) ) ;
#30731=ORIENTED_EDGE ( 'NONE', *, *, #79716, .F. ) ;
#30732=ORIENTED_EDGE ( 'NONE', *, *, #84386, .T. ) ;
#30734=CARTESIAN_POINT ( 'NONE',  ( -92.62287095715008434, -23.73934037231758154, 11.05740245334329153 ) ) ;
#30735=CARTESIAN_POINT ( 'NONE',  ( -77.62287095715007013, -24.66019654487199730, 8.947790411086128159 ) ) ;
#30736=CARTESIAN_POINT ( 'NONE',  ( -36.62287095715005592, -29.50250243563736774, 8.947779886222148704 ) ) ;
#30737=CARTESIAN_POINT ( 'NONE',  ( -92.63388132361646399, -23.96169478059713498, 10.65365249895717881 ) ) ;
#30738=DIRECTION ( 'NONE',  ( -3.773278334453080206E-23, 0.9999999999976377785, 2.173523156925979975E-06 ) ) ;
#30739=CARTESIAN_POINT ( 'NONE',  ( -15.97456084408017674, 15.39233244482803009, 11.49999999999999645 ) ) ;
#30740=ORIENTED_EDGE ( 'NONE', *, *, #77135, .F. ) ;
#30741=DIRECTION ( 'NONE',  ( -3.773278334453079030E-23, 0.9999999999976377785, 2.173523156925979128E-06 ) ) ;
#30742=ORIENTED_EDGE ( 'NONE', *, *, #7552, .F. ) ;
#30743=CARTESIAN_POINT ( 'NONE',  ( -15.40814491850785650, 16.58152744545821022, -1.500000000000002220 ) ) ;
#30744=CARTESIAN_POINT ( 'NONE',  ( -111.5228709571500616, -23.48786465467242479, 11.44779295918253936 ) ) ;
#30748=CARTESIAN_POINT ( 'NONE',  ( -4.889416449700032530, -19.50743224814450016, 11.49999999999998934 ) ) ;
#30749=B_SPLINE_SURFACE_WITH_KNOTS ( 'NONE', 3, 3, ( 
 ( #58845, #59338, #74560, #44614 ),
 ( #75540, #6044, #91282, #42633 ),
 ( #35004, #65985, #96902, #27396 ),
 ( #58356, #89292, #93776, #39500 ),
 ( #24267, #14145, #70449, #77042 ),
 ( #8040, #55241, #14651, #99385 ),
 ( #38498, #45123, #6549, #92768 ) ),
 .UNSPECIFIED., .F., .F., .F.,
 ( 4, 3, 4 ),
 ( 4, 4 ),
 ( 0.7945040050992250302, 0.8970133687736506767, 0.9995227324480763231 ),
 ( 0.4896184160691255394, 0.4908571809756236970 ),
 .UNSPECIFIED. ) ;
#30750=CARTESIAN_POINT ( 'NONE',  ( -80.62287095715005592, -24.83602698348159876, 1.605859176311268399 ) ) ;
#30752=CARTESIAN_POINT ( 'NONE',  ( -92.58953762381672448, -23.48786465467241413, 11.44779295918254469 ) ) ;
#30753=CARTESIAN_POINT ( 'NONE',  ( -18.01732314745861530, 13.19606014829601826, -1.500000000000002220 ) ) ;
#30754=VERTEX_POINT ( 'NONE', #1205 ) ;
#30755=ORIENTED_EDGE ( 'NONE', *, *, #52529, .F. ) ;
#30756=CARTESIAN_POINT ( 'NONE',  ( -101.3987937098823409, -25.25341184233823100, 6.605698944729169853 ) ) ;
#30757=DIRECTION ( 'NONE',  ( -3.773278334453079030E-23, 0.9999999999976377785, 2.173523156925979128E-06 ) ) ;
#30758=EDGE_CURVE ( 'NONE', #58273, #90958, #14518, .T. ) ;
#30760=CARTESIAN_POINT ( 'NONE',  ( -68.52287095715004739, -24.35013146730202749, 9.818937971375110152 ) ) ;
#30761=ADVANCED_FACE ( 'NONE', ( #55490 ), #16404, .T. ) ;
#30763=CARTESIAN_POINT ( 'NONE',  ( 9.052818235119415746, 17.31195010612007223, 11.49999999999998934 ) ) ;
#30765=CARTESIAN_POINT ( 'NONE',  ( -102.5228709571500900, -24.34917612407034682, 0.1852690917477876065 ) ) ;
#30766=CARTESIAN_POINT ( 'NONE',  ( -18.34654256122676941, -11.15389649534839833, -1.500000000000002220 ) ) ;
#30767=CARTESIAN_POINT ( 'NONE',  ( -25.97212670940007584, -24.92774901861465153, 2.712286590796212593 ) ) ;
#30768=ADVANCED_FACE ( 'NONE', ( #32640 ), #38246, .T. ) ;
#30770=CARTESIAN_POINT ( 'NONE',  ( -59.55620429048337883, -23.48783264082478084, -1.443836473390068820 ) ) ;
#30773=CARTESIAN_POINT ( 'NONE',  ( 15.42672287639063100, 16.92133821996916865, -1.500000000000002220 ) ) ;
#30775=CARTESIAN_POINT ( 'NONE',  ( -96.63904445658880604, -23.48786465467241058, 11.44779295918254469 ) ) ;
#30776=CARTESIAN_POINT ( 'NONE',  ( -127.5562042904833930, -23.47593901973091235, -1.443836447538995760 ) ) ;
#30777=CARTESIAN_POINT ( 'NONE',  ( 4.397486433803790007, -19.56896378179033036, 11.49999999999999645 ) ) ;
#30778=CARTESIAN_POINT ( 'NONE',  ( -79.04068788000392942, -25.26612565946948052, 5.390100810327893122 ) ) ;
#30779=CARTESIAN_POINT ( 'NONE',  ( -113.5562042904834072, -24.64965694238575367, 8.947790433994196491 ) ) ;
#30782=CARTESIAN_POINT ( 'NONE',  ( -108.6228709571500559, -23.94994826722515668, -0.6494450866351694218 ) ) ;
#30783=ORIENTED_EDGE ( 'NONE', *, *, #20459, .F. ) ;
#30784=ADVANCED_FACE ( 'NONE', ( #84924 ), #690, .F. ) ;
#30785=CARTESIAN_POINT ( 'NONE',  ( -26.97298592485077506, -24.59688319057676154, 1.763040481647563995 ) ) ;
#30787=CARTESIAN_POINT ( 'NONE',  ( 7.827691340095081607, 20.28360254610759839, 11.49999999999998934 ) ) ;
#30790=CARTESIAN_POINT ( 'NONE',  ( 13.16580039582533423, -14.52177825760336205, -1.500000000000002220 ) ) ;
#30791=CARTESIAN_POINT ( 'NONE',  ( -38.52287095715006870, -23.48786465467241058, 11.44779295918255180 ) ) ;
#30793=CARTESIAN_POINT ( 'NONE',  ( -110.1668890976376360, -25.31698235040695621, 5.541054210284112713 ) ) ;
#30798=CARTESIAN_POINT ( 'NONE',  ( -9.379331868514380943, 18.20734191464070406, 11.49999999999999645 ) ) ;
#30799=LINE ( 'NONE', #61267, #3570 ) ;
#30800=CARTESIAN_POINT ( 'NONE',  ( -120.5166145060558165, -24.92564183028979841, 1.928384488918253536 ) ) ;
#30801=VECTOR ( 'NONE', #58110, 1000.000000000000114 ) ;
#30802=VERTEX_POINT ( 'NONE', #38746 ) ;
#30803=CARTESIAN_POINT ( 'NONE',  ( -99.72794805030189025, -25.26387389937925576, 4.442265393084401381 ) ) ;
#30804=CARTESIAN_POINT ( 'NONE',  ( -39.56145255469812128, -25.18430974075399575, 3.766659751673692380 ) ) ;
#30806=CARTESIAN_POINT ( 'NONE',  ( -85.62287095714999907, -24.15431212366391378, -0.2830839119429074402 ) ) ;
#30807=CARTESIAN_POINT ( 'NONE',  ( -25.54628175542703161, -24.61459516021406913, 5.501431625134629577 ) ) ;
#30809=EDGE_CURVE ( 'NONE', #80599, #46090, #77406, .T. ) ;
#30810=CARTESIAN_POINT ( 'NONE',  ( -13.16640216892762894, -18.94680327863774849, 11.49999999999999645 ) ) ;
#30811=CARTESIAN_POINT ( 'NONE',  ( -10.93939140624874007, -20.02795264745160608, 11.49999999999998934 ) ) ;
#30812=CARTESIAN_POINT ( 'NONE',  ( -74.60678690070801622, -23.48783264082477018, -1.443836473390096353 ) ) ;
#30813=CARTESIAN_POINT ( 'NONE',  ( -88.52287095715001897, -24.34917612406836795, 0.1852690917426557116 ) ) ;
#30815=CARTESIAN_POINT ( 'NONE',  ( 9.841385673706204429, 20.17164819615926064, 11.49999999999999645 ) ) ;
#30817=CARTESIAN_POINT ( 'NONE',  ( -100.6228709571500275, -24.52232992886363405, 0.6492154411906175815 ) ) ;
#30818=CARTESIAN_POINT ( 'NONE',  ( -43.65487935057238644, -23.73766607897671221, -1.055555164236442689 ) ) ;
#30819=CARTESIAN_POINT ( 'NONE',  ( 14.12621959167996977, 16.79361087625908056, 11.49999999999998934 ) ) ;
#30820=EDGE_CURVE ( 'NONE', #97261, #100338, #36281, .T. ) ;
#30821=B_SPLINE_CURVE_WITH_KNOTS ( 'NONE', 3,
 ( #28474, #92746, #31359, #54711, #90380, #7019 ),
 .UNSPECIFIED., .F., .F.,
 ( 4, 2, 4 ),
 ( 0.000000000000000000, 0.001380901958385392448, 0.002761803916770784895 ),
 .UNSPECIFIED. ) ;
#30822=CARTESIAN_POINT ( 'NONE',  ( -98.52287095715009002, -24.66019654487200441, 8.947790411086119278 ) ) ;
#30823=CARTESIAN_POINT ( 'NONE',  ( -87.55455836477378284, -23.96169478059713498, 10.65365249895718058 ) ) ;
#30824=CARTESIAN_POINT ( 'NONE',  ( -40.66986802185439132, -25.31545374197336074, 5.060077358709395234 ) ) ;
#30825=CARTESIAN_POINT ( 'NONE',  ( -78.60556800691774981, -23.48783264082477018, -1.443836473390096797 ) ) ;
#30827=VERTEX_POINT ( 'NONE', #88937 ) ;
#30828=CARTESIAN_POINT ( 'NONE',  ( 5.889875310795558150, 19.62242631308348706, -1.500000000000002220 ) ) ;
#30829=VERTEX_POINT ( 'NONE', #19414 ) ;
#30830=ORIENTED_EDGE ( 'NONE', *, *, #54196, .F. ) ;
#30833=CARTESIAN_POINT ( 'NONE',  ( -18.41700849636773540, 13.91914711744011157, -1.500000000000002220 ) ) ;
#30834=CARTESIAN_POINT ( 'NONE',  ( -45.52287095715006160, -24.99132157543083821, 2.256160258750667502 ) ) ;
#30835=CARTESIAN_POINT ( 'NONE',  ( -18.13051092187696156, -9.059970205480309957, -1.500000000000002220 ) ) ;
#30837=CARTESIAN_POINT ( 'NONE',  ( -115.5228709571500474, -23.47593901973090524, -1.443836447538996204 ) ) ;
#30838=CARTESIAN_POINT ( 'NONE',  ( -92.52216719015747515, -23.48783264082477729, -1.443836473390063713 ) ) ;
#30839=CARTESIAN_POINT ( 'NONE',  ( -101.2821955461997732, -25.18596798425043559, 6.774419534272953847 ) ) ;
#30840=CARTESIAN_POINT ( 'NONE',  ( -70.49528693087628994, -24.63355581998385091, 0.9682620441943861067 ) ) ;
#30841=CARTESIAN_POINT ( 'NONE',  ( 8.900169022907615357, -19.58186849131130813, 11.49999999999999645 ) ) ;
#30842=ORIENTED_EDGE ( 'NONE', *, *, #92389, .T. ) ;
#30843=CARTESIAN_POINT ( 'NONE',  ( -79.52287095715006160, -24.66019654487199375, 8.947790411086122830 ) ) ;
#30844=CARTESIAN_POINT ( 'NONE',  ( -49.10457154551148307, -25.31573627678961103, 3.999772159320571063 ) ) ;
#30846=CARTESIAN_POINT ( 'NONE',  ( 20.64725891757762355, 2.036748910689437864, -1.500000000000002220 ) ) ;
#30853=ORIENTED_EDGE ( 'NONE', *, *, #29190, .F. ) ;
#30856=CARTESIAN_POINT ( 'NONE',  ( -42.60799034082329229, -23.73791477778911485, 11.05961554403171299 ) ) ;
#30857=CARTESIAN_POINT ( 'NONE',  ( -65.63886145207663958, -24.40034930558990922, 0.3402023900116040167 ) ) ;
#30858=CARTESIAN_POINT ( 'NONE',  ( -11.46427080702723522, -18.74017919159951973, 11.49999999999999645 ) ) ;
#30860=CARTESIAN_POINT ( 'NONE',  ( 22.54279463279464579, 0.6884863543687869125, -1.500000000000002220 ) ) ;
#30861=CARTESIAN_POINT ( 'NONE',  ( -12.80012119340476140, -16.60591428456014640, -1.500000000000002220 ) ) ;
#30862=CARTESIAN_POINT ( 'NONE',  ( -89.62287095715002749, -24.50216790748206108, 0.6166512839542551694 ) ) ;
#30868=EDGE_LOOP ( 'NONE', ( #15597, #55612, #42285, #27739 ) ) ;
#30870=AXIS2_PLACEMENT_3D ( 'NONE', #93282, #33388, #94789 ) ;
#30871=CARTESIAN_POINT ( 'NONE',  ( -21.45671390985790694, -1.711987587955616119, -1.500000000000002220 ) ) ;
#30872=CARTESIAN_POINT ( 'NONE',  ( -114.5562042904834072, -23.47593901973091235, -1.443836447538999312 ) ) ;
#30874=CARTESIAN_POINT ( 'NONE',  ( 6.572693220633653688, -20.11273663914708365, -1.500000000000002220 ) ) ;
#30875=LINE ( 'NONE', #92762, #57921 ) ;
#30876=PLANE ( 'NONE',  #49527 ) ;
#30877=DIRECTION ( 'NONE',  ( 0.000000000000000000, -0.8406134417706465634, -0.5416355246053453643 ) ) ;
#30878=DIRECTION ( 'NONE',  ( 0.000000000000000000, 2.173523156925980399E-06, -0.9999999999976378895 ) ) ;
#30879=CARTESIAN_POINT ( 'NONE',  ( -47.62287095715006302, -23.47596703998600276, 11.44779298504227505 ) ) ;
#30880=CARTESIAN_POINT ( 'NONE',  ( -21.14524153552446606, 6.695245452574716261, -1.500000000000002220 ) ) ;
#30881=CARTESIAN_POINT ( 'NONE',  ( -80.62287095715007013, -25.00158670708909625, 2.256160236439165967 ) ) ;
#30883=ORIENTED_EDGE ( 'NONE', *, *, #63135, .F. ) ;
#30886=CARTESIAN_POINT ( 'NONE',  ( -126.6234820361467825, -24.65952944569305316, 1.056160979905705455 ) ) ;
#30888=CARTESIAN_POINT ( 'NONE',  ( 16.20606029192996900, -10.75321813762353251, -1.500000000000002220 ) ) ;
#30890=CARTESIAN_POINT ( 'NONE',  ( -14.55006661338671847, 15.66751491618662406, 11.49999999999998934 ) ) ;
#30891=CARTESIAN_POINT ( 'NONE',  ( -62.58331733608945058, -24.51314013834316441, 0.6176544820404141767 ) ) ;
#30893=EDGE_CURVE ( 'NONE', #71598, #10587, #79312, .T. ) ;
#30894=CARTESIAN_POINT ( 'NONE',  ( -79.62287095715011276, -24.34917612406837861, 0.1852690917426644546 ) ) ;
#30896=CARTESIAN_POINT ( 'NONE',  ( -5.639450322166912777, -21.95568564230989850, -1.500000000000002220 ) ) ;
#30899=CARTESIAN_POINT ( 'NONE',  ( -12.84220538718065185, 15.17226672225704398, 11.49999999999999645 ) ) ;
#30902=ADVANCED_FACE ( 'NONE', ( #41265 ), #41779, .T. ) ;
#30906=CARTESIAN_POINT ( 'NONE',  ( 11.52859134480388903, -18.33581920571378632, 11.49999999999998934 ) ) ;
#30907=PLANE ( 'NONE',  #85256 ) ;
#30908=CARTESIAN_POINT ( 'NONE',  ( 18.36381783059253081, 6.383776564742674964, -1.500000000000002220 ) ) ;
#30909=CARTESIAN_POINT ( 'NONE',  ( -114.6228709571500559, -24.64965695001469115, 8.947790433994176951 ) ) ;
#30910=CARTESIAN_POINT ( 'NONE',  ( -55.57730503950245549, -24.92592662359560762, 8.075495903017996469 ) ) ;
#30911=CARTESIAN_POINT ( 'NONE',  ( -9.134819693115781902, 17.59984377705169933, 11.49999999999998934 ) ) ;
#30912=VERTEX_POINT ( 'NONE', #88439 ) ;
#30913=CARTESIAN_POINT ( 'NONE',  ( 14.62039552936377085, -14.08751720214925207, 11.49999999999999645 ) ) ;
#30914=CARTESIAN_POINT ( 'NONE',  ( -80.56574368191338920, -23.48783264082477018, -1.443836473390096131 ) ) ;
#30915=VECTOR ( 'NONE', #95506, 1000.000000000000114 ) ;
#30918=CARTESIAN_POINT ( 'NONE',  ( -0.03676920774744678322, -22.57399371096969531, 8.369064737642425200 ) ) ;
#30919=FACE_OUTER_BOUND ( 'NONE', #36987, .T. ) ;
#30920=CARTESIAN_POINT ( 'NONE',  ( -49.20147844880023058, -25.25214510237312737, 5.321223747615992039 ) ) ;
#30921=CARTESIAN_POINT ( 'NONE',  ( -40.53339838483739044, -24.63419186844611630, 9.035850630976923981 ) ) ;
#30922=PLANE ( 'NONE',  #43038 ) ;
#30923=CARTESIAN_POINT ( 'NONE',  ( 18.99975792849237877, 6.539580213093530325, 11.49999999999998934 ) ) ;
#30925=CARTESIAN_POINT ( 'NONE',  ( -89.62287095715004170, -24.66019654487199020, 8.947790411086128159 ) ) ;
#30926=ORIENTED_EDGE ( 'NONE', *, *, #25034, .F. ) ;
#30927=CARTESIAN_POINT ( 'NONE',  ( -129.5228709571500758, -23.47593901973090524, -1.443836447538996204 ) ) ;
#30929=CARTESIAN_POINT ( 'NONE',  ( -15.36296916364455711, -16.94538937337987150, 11.49999999999999645 ) ) ;
#30930=CARTESIAN_POINT ( 'NONE',  ( -13.93578158028743985, 17.96481793202167054, -1.500000000000002220 ) ) ;
#30931=VERTEX_POINT ( 'NONE', #9806 ) ;
#30932=CARTESIAN_POINT ( 'NONE',  ( -109.6228709571500701, -23.73907113216991860, -1.053371485793223261 ) ) ;
#30934=CARTESIAN_POINT ( 'NONE',  ( -38.62892889660167839, -24.51419770103157703, 9.386484678747176957 ) ) ;
#30936=CARTESIAN_POINT ( 'NONE',  ( -49.52287095715006160, -23.48783264082477018, -1.443836473390095465 ) ) ;
#30937=FACE_OUTER_BOUND ( 'NONE', #54381, .T. ) ;
#30939=CARTESIAN_POINT ( 'NONE',  ( -111.6228709571500843, -23.47596703998600631, 11.44779298504227860 ) ) ;
#30940=VERTEX_POINT ( 'NONE', #64125 ) ;
#30941=CARTESIAN_POINT ( 'NONE',  ( 15.88337727998148985, 12.78846505907953279, 11.49999999999998934 ) ) ;
#30943=B_SPLINE_CURVE_WITH_KNOTS ( 'NONE', 3,
 ( #60792, #16588, #2388, #38934 ),
 .UNSPECIFIED., .F., .F.,
 ( 4, 4 ),
 ( 0.000000000000000000, 9.999999999994735322E-05 ),
 .UNSPECIFIED. ) ;
#30944=CARTESIAN_POINT ( 'NONE',  ( 8.272623322502495213, 21.45567517505680044, 11.49999999999998934 ) ) ;
#30945=CARTESIAN_POINT ( 'NONE',  ( -103.6228709571500701, -23.48783264082478794, -1.443836473390062158 ) ) ;
#30946=ORIENTED_EDGE ( 'NONE', *, *, #17382, .T. ) ;
#30947=FACE_OUTER_BOUND ( 'NONE', #4822, .T. ) ;
#30948=B_SPLINE_CURVE_WITH_KNOTS ( 'NONE', 3,
 ( #25945, #10222, #17839, #88350, #11222, #26456 ),
 .UNSPECIFIED., .F., .F.,
 ( 4, 2, 4 ),
 ( 6.384118678613282972E-06, 0.001386860460828377153, 0.002767336802978141025 ),
 .UNSPECIFIED. ) ;
#30950=CARTESIAN_POINT ( 'NONE',  ( -51.60612219431600778, -23.73791477778912196, 11.05961554403170766 ) ) ;
#30951=CARTESIAN_POINT ( 'NONE',  ( -14.73150212448299357, 15.28860238833873808, 11.49999999999999645 ) ) ;
#30954=CARTESIAN_POINT ( 'NONE',  ( 17.16062296631688255, 14.07911611715085876, -1.500000000000002220 ) ) ;
#30955=CARTESIAN_POINT ( 'NONE',  ( -15.40095275084150117, -13.70674696055758801, -1.500000000000002220 ) ) ;
#30957=ORIENTED_EDGE ( 'NONE', *, *, #62782, .F. ) ;
#30958=ORIENTED_EDGE ( 'NONE', *, *, #92916, .T. ) ;
#30959=CARTESIAN_POINT ( 'NONE',  ( -109.8650282762807393, -25.27682926508576955, 5.784628013120847179 ) ) ;
#30961=ORIENTED_EDGE ( 'NONE', *, *, #94445, .T. ) ;
#30963=EDGE_CURVE ( 'NONE', #14386, #65949, #31219, .T. ) ;
#30964=ORIENTED_EDGE ( 'NONE', *, *, #71946, .T. ) ;
#30965=CARTESIAN_POINT ( 'NONE',  ( -121.5562042904834072, -23.47596703998600631, 11.44779298504227683 ) ) ;
#30966=FACE_OUTER_BOUND ( 'NONE', #42957, .T. ) ;
#30967=CARTESIAN_POINT ( 'NONE',  ( 13.71216040526616098, 15.69570726272272232, -1.500000000000002220 ) ) ;
#30968=CARTESIAN_POINT ( 'NONE',  ( -21.33044368757495590, -4.375833669458513597, 11.49999999999999645 ) ) ;
#30970=CARTESIAN_POINT ( 'NONE',  ( -78.60051775479411162, -23.73791477778911840, 11.05961554403170588 ) ) ;
#30971=CARTESIAN_POINT ( 'NONE',  ( -12.88509029660790617, -18.40938060607246740, -1.500000000000002220 ) ) ;
#30972=EDGE_CURVE ( 'NONE', #24356, #58437, #65237, .T. ) ;
#30978=EDGE_CURVE ( 'NONE', #49308, #23684, #49396, .T. ) ;
#30979=ORIENTED_EDGE ( 'NONE', *, *, #98781, .T. ) ;
#30980=ORIENTED_EDGE ( 'NONE', *, *, #90093, .F. ) ;
#30981=AXIS2_PLACEMENT_3D ( 'NONE', #39520, #86191, #95306 ) ;
#30983=CARTESIAN_POINT ( 'NONE',  ( -19.36244235409943926, 8.944087295975924334, -1.500000000000002220 ) ) ;
#30984=ORIENTED_EDGE ( 'NONE', *, *, #23659, .T. ) ;
#30985=CARTESIAN_POINT ( 'NONE',  ( -6.845587600281468177, 19.88882266644084496, 11.49999999999998934 ) ) ;
#30986=DIRECTION ( 'NONE',  ( 1.000000000000000000, 3.773278334444167608E-23, 8.201307833595939069E-29 ) ) ;
#30988=CARTESIAN_POINT ( 'NONE',  ( -55.52287095715008292, -23.47593901973090169, -1.443836447538997092 ) ) ;
#30989=CARTESIAN_POINT ( 'NONE',  ( -49.41232686713205169, -25.10396340747056598, 7.262126897097727962 ) ) ;
#30990=CARTESIAN_POINT ( 'NONE',  ( 9.413913215453616701, -19.89622248225912315, -1.500000000000002220 ) ) ;
#30992=VERTEX_POINT ( 'NONE', #17926 ) ;
#30995=CARTESIAN_POINT ( 'NONE',  ( -49.10457154551148307, -25.26416398485831749, 3.999772271414141489 ) ) ;
#30996=CARTESIAN_POINT ( 'NONE',  ( -19.94048968823238255, 6.179419890754223488, 11.49999999999999645 ) ) ;
#30999=CARTESIAN_POINT ( 'NONE',  ( -108.6228709571500417, -24.66019654487199730, 8.947790411086124607 ) ) ;
#31000=CARTESIAN_POINT ( 'NONE',  ( -10.24605875044832182, -22.99950505309962523, 9.174899246800714891 ) ) ;
#31001=CARTESIAN_POINT ( 'NONE',  ( 9.569808575145499319, 19.01914523534739132, 11.49999999999998934 ) ) ;
#31002=CARTESIAN_POINT ( 'NONE',  ( -31.24388727629347784, -25.26956746990935443, 6.087265963545713809 ) ) ;
#31003=CARTESIAN_POINT ( 'NONE',  ( -107.5967350901245254, -23.48786465467241413, 11.44779295918253759 ) ) ;
#31005=CARTESIAN_POINT ( 'NONE',  ( -90.62287095715005592, -24.91544648472620693, 1.928969306349234802 ) ) ;
#31006=CARTESIAN_POINT ( 'NONE',  ( -69.33027971892866503, -25.28687673834294003, 5.910757521653128066 ) ) ;
#31007=CARTESIAN_POINT ( 'NONE',  ( 0.003324065884441271702, 22.49086686382009503, -1.500000000000002220 ) ) ;
#31008=EDGE_CURVE ( 'NONE', #59593, #21715, #9481, .T. ) ;
#31009=CARTESIAN_POINT ( 'NONE',  ( -108.8769404936500109, -25.25626643526282322, 3.571638612575483318 ) ) ;
#31011=CARTESIAN_POINT ( 'NONE',  ( -49.62287095715005592, -24.64965695001467694, 8.947790433994185832 ) ) ;
#31012=CARTESIAN_POINT ( 'NONE',  ( 9.307004028210867475, 17.29072351678862418, 11.49999999999999645 ) ) ;
#31013=DIRECTION ( 'NONE',  ( 3.773278334444166432E-23, -1.000000000000000000, 0.000000000000000000 ) ) ;
#31015=ORIENTED_EDGE ( 'NONE', *, *, #84916, .F. ) ;
#31016=EDGE_CURVE ( 'NONE', #54879, #7016, #73641, .T. ) ;
#31017=CARTESIAN_POINT ( 'NONE',  ( -69.84206102715404541, -25.30531021297771233, 4.913976341363863298 ) ) ;
#31018=CARTESIAN_POINT ( 'NONE',  ( -95.52287095715006160, -29.50250786944525672, 11.44777988621623166 ) ) ;
#31019=CARTESIAN_POINT ( 'NONE',  ( -88.86938553902136562, -25.32379766982192493, 4.367815445636562544 ) ) ;
#31020=ADVANCED_FACE ( 'NONE', ( #58498 ), #89433, .F. ) ;
#31021=CARTESIAN_POINT ( 'NONE',  ( 16.04393857186779115, -11.51807295290239885, 11.49999999999998934 ) ) ;
#31024=CARTESIAN_POINT ( 'NONE',  ( -120.5228709571499905, -24.15516710230294706, 10.28746687063725496 ) ) ;
#31025=VECTOR ( 'NONE', #27138, 1000.000000000000114 ) ;
#31029=CARTESIAN_POINT ( 'NONE',  ( -48.62287095715006302, -24.50321055353803601, 9.387540953477527594 ) ) ;
#31030=CARTESIAN_POINT ( 'NONE',  ( -55.47781443094807230, -25.00158670708910336, 2.256160236439221034 ) ) ;
#31031=CARTESIAN_POINT ( 'NONE',  ( -99.20586904084365187, -25.03145057151672148, 7.003177191084415831 ) ) ;
#31032=DIRECTION ( 'NONE',  ( -3.773278334444167608E-23, 1.000000000000000000, 0.000000000000000000 ) ) ;
#31033=CARTESIAN_POINT ( 'NONE',  ( -56.55620429048340014, -24.65952944569304606, 1.056160979905696129 ) ) ;
#31035=CARTESIAN_POINT ( 'NONE',  ( -12.72357806474857966, 15.40231687525621318, -1.500000000000002220 ) ) ;
#31039=CARTESIAN_POINT ( 'NONE',  ( -79.59586937953757513, -23.96169478059713143, 10.65365249895718058 ) ) ;
#31040=CARTESIAN_POINT ( 'NONE',  ( -109.5745106736623029, -25.18430227007843669, 3.630693441492102824 ) ) ;
#31041=CARTESIAN_POINT ( 'NONE',  ( -35.66629527092394625, -23.85016227208580730, -0.8807180028928173199 ) ) ;
#31047=PLANE ( 'NONE',  #40440 ) ;
#31049=CARTESIAN_POINT ( 'NONE',  ( 0.8729654516333695824, -20.24016528753796962, 11.49999999999998934 ) ) ;
#31050=CARTESIAN_POINT ( 'NONE',  ( -109.5895376238167103, -23.48783264082478794, -1.443836473390060382 ) ) ;
#31051=CARTESIAN_POINT ( 'NONE',  ( -99.62287095715005592, -23.47593901973091235, -1.443836447539001089 ) ) ;
#31054=VECTOR ( 'NONE', #14293, 1000.000000000000227 ) ;
#31055=CARTESIAN_POINT ( 'NONE',  ( 20.09017895974002599, 0.4902201509063087159, -1.500000000000002220 ) ) ;
#31056=CARTESIAN_POINT ( 'NONE',  ( -1.999300432013352058, 20.99099883833691749, 11.49999999999999645 ) ) ;
#31057=AXIS2_PLACEMENT_3D ( 'NONE', #2652, #94981, #62542 ) ;
#31058=CARTESIAN_POINT ( 'NONE',  ( 22.05266032001784637, -1.487345182339283367, -1.500000000000002220 ) ) ;
#31059=CARTESIAN_POINT ( 'NONE',  ( -13.21525772315781388, 15.71049578022273785, -1.500000000000002220 ) ) ;
#31060=CARTESIAN_POINT ( 'NONE',  ( -122.5228709571500616, -24.66019654487200441, 8.947790411086112172 ) ) ;
#31062=B_SPLINE_CURVE_WITH_KNOTS ( 'NONE', 3,
 ( #29310, #21681, #23183, #8477 ),
 .UNSPECIFIED., .F., .F.,
 ( 4, 4 ),
 ( 0.9611863596518752662, 0.9701927909239907999 ),
 .UNSPECIFIED. ) ;
#31065=PLANE ( 'NONE',  #94645 ) ;
#31068=CARTESIAN_POINT ( 'NONE',  ( -64.62287095715005592, -24.64965695001468404, 8.947790433994185832 ) ) ;
#31069=VERTEX_POINT ( 'NONE', #43268 ) ;
#31071=ORIENTED_EDGE ( 'NONE', *, *, #56157, .F. ) ;
#31074=CARTESIAN_POINT ( 'NONE',  ( -77.58953762381672448, -24.65952944569304606, 1.056160979905698794 ) ) ;
#31075=CARTESIAN_POINT ( 'NONE',  ( 1.453578435135240321, -20.60874541997745268, -1.500000000000002220 ) ) ;
#31076=CARTESIAN_POINT ( 'NONE',  ( 17.73057777116804701, 12.32922261165129285, 11.49999999999999645 ) ) ;
#31077=ORIENTED_EDGE ( 'NONE', *, *, #100121, .F. ) ;
#31078=EDGE_CURVE ( 'NONE', #55585, #89617, #59101, .T. ) ;
#31080=CARTESIAN_POINT ( 'NONE',  ( -60.62287095715006302, -24.51163499207174468, 0.6490370598554270343 ) ) ;
#31081=CARTESIAN_POINT ( 'NONE',  ( -21.16225983376422448, 7.283793490815352989, 11.49999999999998934 ) ) ;
#31082=EDGE_CURVE ( 'NONE', #89004, #17644, #37354, .T. ) ;
#31083=EDGE_CURVE ( 'NONE', #84745, #11381, #96643, .T. ) ;
#31084=CARTESIAN_POINT ( 'NONE',  ( -79.36551648466291908, -25.12205614543422172, 6.194054221785125769 ) ) ;
#31085=CARTESIAN_POINT ( 'NONE',  ( -53.52287095715009002, -24.33832256527048088, 0.1851278514138568754 ) ) ;
#31087=FACE_OUTER_BOUND ( 'NONE', #21675, .T. ) ;
#31088=CARTESIAN_POINT ( 'NONE',  ( -49.48966588299922620, -24.51419770103158413, 9.386484678747189392 ) ) ;
#31089=EDGE_CURVE ( 'NONE', #75416, #13388, #55500, .T. ) ;
#31090=CARTESIAN_POINT ( 'NONE',  ( -115.5228709571501042, -23.84047902841602351, -0.8780736468305720965 ) ) ;
#31091=CARTESIAN_POINT ( 'NONE',  ( 17.12911088700535700, -11.98135219954639830, 11.49999999999998934 ) ) ;
#31094=VERTEX_POINT ( 'NONE', #44761 ) ;
#31095=B_SPLINE_CURVE_WITH_KNOTS ( 'NONE', 3,
 ( #41354, #87021, #33742, #18011 ),
 .UNSPECIFIED., .F., .F.,
 ( 4, 4 ),
 ( 0.000000000000000000, 9.999999999998897304E-05 ),
 .UNSPECIFIED. ) ;
#31097=CARTESIAN_POINT ( 'NONE',  ( -109.5922553255047660, -23.96169478059713853, 10.65365249895717703 ) ) ;
#31098=CARTESIAN_POINT ( 'NONE',  ( -18.51692787870624102, -10.26217664800131502, -1.500000000000002220 ) ) ;
#31099=ORIENTED_EDGE ( 'NONE', *, *, #78848, .F. ) ;
#31101=CARTESIAN_POINT ( 'NONE',  ( -21.76810506448615712, 0.6044244127108716613, -1.500000000000002220 ) ) ;
#31102=PLANE ( 'NONE',  #70806 ) ;
#31105=CARTESIAN_POINT ( 'NONE',  ( 6.392671032147439369, 20.83241601264130693, -1.500000000000002220 ) ) ;
#31106=CARTESIAN_POINT ( 'NONE',  ( -95.52287095715013265, -24.83602698348160231, 1.605859176311266179 ) ) ;
#31107=EDGE_LOOP ( 'NONE', ( #1651, #53785, #91155, #16562 ) ) ;
#31108=DIRECTION ( 'NONE',  ( 0.000000000000000000, -2.173523156925979552E-06, 0.9999999999976378895 ) ) ;
#31115=CARTESIAN_POINT ( 'NONE',  ( -72.52287095715007581, -29.50247984919015209, -1.443849546365055359 ) ) ;
#31116=CARTESIAN_POINT ( 'NONE',  ( -44.62287095715004881, -24.64898659630528854, 1.056161002820819261 ) ) ;
#31117=CARTESIAN_POINT ( 'NONE',  ( 21.17954554857512761, 0.9134790845329443520, 11.49999999999998934 ) ) ;
#31119=CARTESIAN_POINT ( 'NONE',  ( -121.6228709571500417, -23.72747288104441665, -1.053458166803660445 ) ) ;
#31120=CARTESIAN_POINT ( 'NONE',  ( -79.88583274576632220, -25.03138275433761706, 7.452192808739267704 ) ) ;
#31124=CARTESIAN_POINT ( 'NONE',  ( 19.05472526407214673, 3.605321472892077050, 11.49999999999998934 ) ) ;
#31125=CARTESIAN_POINT ( 'NONE',  ( -51.92991042017824554, -25.26556399697136968, 6.106724579306912482 ) ) ;
#31127=CARTESIAN_POINT ( 'NONE',  ( 7.440116899146960172, 17.95454168335740874, 11.49999999999999645 ) ) ;
#31128=CARTESIAN_POINT ( 'NONE',  ( -126.5228709571500616, -23.47596703998600631, 11.44779298504227683 ) ) ;
#31130=ORIENTED_EDGE ( 'NONE', *, *, #80690, .T. ) ;
#31133=CARTESIAN_POINT ( 'NONE',  ( -70.66311671602751687, -25.30500184331102886, 4.882606927408491337 ) ) ;
#31134=CARTESIAN_POINT ( 'NONE',  ( -64.62287095715011276, -23.94994826722565762, -0.6494450866342728057 ) ) ;
#31136=B_SPLINE_CURVE_WITH_KNOTS ( 'NONE', 3,
 ( #95193, #3366, #50518, #26686 ),
 .UNSPECIFIED., .F., .F.,
 ( 4, 4 ),
 ( 0.000000000000000000, 9.999999999998897304E-05 ),
 .UNSPECIFIED. ) ;
#31137=VECTOR ( 'NONE', #51613, 1000.000000000000114 ) ;
#31138=CARTESIAN_POINT ( 'NONE',  ( -55.62287095715004881, -23.48783264082478084, -1.443836473390068820 ) ) ;
#31139=CARTESIAN_POINT ( 'NONE',  ( -3.832734262880480358, 19.25313627021017382, -1.500000000000002220 ) ) ;
#31140=CARTESIAN_POINT ( 'NONE',  ( -35.62287095715005592, -29.50248789122583659, 2.256150453626215580 ) ) ;
#31142=ORIENTED_EDGE ( 'NONE', *, *, #7060, .F. ) ;
#31143=CARTESIAN_POINT ( 'NONE',  ( 17.73057777116804701, 12.32922261165129285, 11.49999999999998934 ) ) ;
#31148=CARTESIAN_POINT ( 'NONE',  ( -14.43837761634077310, -17.93274050997184332, -1.500000000000002220 ) ) ;
#31150=CARTESIAN_POINT ( 'NONE',  ( -93.55196295890371516, -24.15543982623907837, -0.2315651400026621232 ) ) ;
#31152=CARTESIAN_POINT ( 'NONE',  ( -121.5556932203309799, -23.96169478059713853, 10.65365249895717525 ) ) ;
#31154=CARTESIAN_POINT ( 'NONE',  ( -111.6050501299251323, -25.29823978627861791, 3.602891629172883636 ) ) ;
#31155=CARTESIAN_POINT ( 'NONE',  ( -63.62287095715004881, -24.64965695001468404, 8.947790433994185832 ) ) ;
#31157=CARTESIAN_POINT ( 'NONE',  ( 11.60740158406642664, -16.16820694497113564, 11.49999999999998934 ) ) ;
#31159=CARTESIAN_POINT ( 'NONE',  ( 3.337697395173636394, -19.57427954046807983, -1.500000000000002220 ) ) ;
#31161=DIRECTION ( 'NONE',  ( -3.773278334453079618E-23, 0.9999999999976377785, 2.173523156925979975E-06 ) ) ;
#31163=CARTESIAN_POINT ( 'NONE',  ( 6.562613027033147084, 19.67253995144353240, 11.49999999999999645 ) ) ;
#31164=DIRECTION ( 'NONE',  ( 1.000000000000000000, 3.773278334444167608E-23, 8.201307833595939069E-29 ) ) ;
#31166=CARTESIAN_POINT ( 'NONE',  ( 6.135622925040504327, -21.92205258971886650, 11.49999999999999645 ) ) ;
#31168=ORIENTED_EDGE ( 'NONE', *, *, #31661, .F. ) ;
#31169=CARTESIAN_POINT ( 'NONE',  ( -83.62287095715009855, -23.73934037231757443, 11.05740245334328975 ) ) ;
#31170=B_SPLINE_CURVE_WITH_KNOTS ( 'NONE', 3,
 ( #65602, #3685, #3195, #20379, #50360, #89412, #97021, #66105 ),
 .UNSPECIFIED., .F., .F.,
 ( 4, 2, 2, 4 ),
 ( -0.001224873891641420440, -0.0002244903592271052430, 0.0007758931731872099544, 0.002776660238015836880 ),
 .UNSPECIFIED. ) ;
#31171=CARTESIAN_POINT ( 'NONE',  ( -92.52287095715006160, -24.64965694238407323, 8.947790433994196491 ) ) ;
#31173=CARTESIAN_POINT ( 'NONE',  ( 19.91930514195032487, 3.327535025408205893, 11.49999999999998934 ) ) ;
#31174=CARTESIAN_POINT ( 'NONE',  ( -108.6228709571500417, -24.50321055353805022, 9.387540953477527594 ) ) ;
#31175=DIRECTION ( 'NONE',  ( 0.000000000000000000, 2.173523156925980399E-06, -0.9999999999976378895 ) ) ;
#31177=ORIENTED_EDGE ( 'NONE', *, *, #97955, .T. ) ;
#31179=CARTESIAN_POINT ( 'NONE',  ( 6.305670413343573699, 22.00876638805999974, 11.49999999999998934 ) ) ;
#31180=CARTESIAN_POINT ( 'NONE',  ( -41.57697449856503624, -25.20347274299025031, 3.352851794561174437 ) ) ;
#31181=CARTESIAN_POINT ( 'NONE',  ( -19.28869470675124731, 9.786980993800005635, -1.500000000000002220 ) ) ;
#31182=CARTESIAN_POINT ( 'NONE',  ( -123.5542534380672919, -24.51314013834318217, 0.6176544820404261671 ) ) ;
#31183=VECTOR ( 'NONE', #28414, 1000.000000000000114 ) ;
#31184=CARTESIAN_POINT ( 'NONE',  ( -19.94816486946033507, 6.322790147265108018, 11.49999999999999645 ) ) ;
#31185=ORIENTED_EDGE ( 'NONE', *, *, #9377, .F. ) ;
#31186=CARTESIAN_POINT ( 'NONE',  ( -69.53040046975404209, -25.31612467077423290, 5.066170237949151556 ) ) ;
#31187=CARTESIAN_POINT ( 'NONE',  ( -20.26759042640731323, -8.618136523154847239, -1.500000000000002220 ) ) ;
#31190=VERTEX_POINT ( 'NONE', #41030 ) ;
#31193=ORIENTED_EDGE ( 'NONE', *, *, #29975, .T. ) ;
#31195=EDGE_CURVE ( 'NONE', #99951, #44074, #32488, .T. ) ;
#31197=EDGE_CURVE ( 'NONE', #73248, #27537, #9066, .T. ) ;
#31198=EDGE_LOOP ( 'NONE', ( #30980, #41449, #60397, #4998 ) ) ;
#31199=CARTESIAN_POINT ( 'NONE',  ( -41.55620429048339304, -24.64965694238574656, 8.947790433994205372 ) ) ;
#31200=CARTESIAN_POINT ( 'NONE',  ( -101.7007079832508367, -25.27404824587932097, 3.725872426325841147 ) ) ;
#31202=CARTESIAN_POINT ( 'NONE',  ( -4.302178748239556150, -20.00421716419250373, -1.500000000000002220 ) ) ;
#31203=ADVANCED_FACE ( 'NONE', ( #86688 ), #78058, .T. ) ;
#31204=ORIENTED_EDGE ( 'NONE', *, *, #47186, .T. ) ;
#31206=CARTESIAN_POINT ( 'NONE',  ( -33.62287095715005592, -23.48786465467240347, 11.44779295918255535 ) ) ;
#31207=DIRECTION ( 'NONE',  ( -3.773278334453079618E-23, 0.9999999999976377785, 2.173523156925979975E-06 ) ) ;
#31208=CARTESIAN_POINT ( 'NONE',  ( 20.12748746789148413, 9.599020362109589755, 11.49999999999998934 ) ) ;
#31209=EDGE_CURVE ( 'NONE', #90352, #45280, #17175, .T. ) ;
#31213=ORIENTED_EDGE ( 'NONE', *, *, #95650, .F. ) ;
#31214=B_SPLINE_CURVE_WITH_KNOTS ( 'NONE', 3,
 ( #89097, #26698, #34810, #57658, #57167, #49049 ),
 .UNSPECIFIED., .F., .F.,
 ( 4, 2, 4 ),
 ( 0.000000000000000000, 0.001380901958385397869, 0.002761803916770795737 ),
 .UNSPECIFIED. ) ;
#31216=CARTESIAN_POINT ( 'NONE',  ( -29.39543059329891506, -24.63645834301326332, 7.191773098902599415 ) ) ;
#31218=CARTESIAN_POINT ( 'NONE',  ( 0.5783248939474509021, 20.82821387695577187, 11.49999999999998934 ) ) ;
#31219=B_SPLINE_CURVE_WITH_KNOTS ( 'NONE', 3,
 ( #87936, #58005, #56504, #42289, #97042, #2213, #25534, #64630 ),
 .UNSPECIFIED., .F., .F.,
 ( 4, 2, 2, 4 ),
 ( 6.384118678613149141E-06, 0.002007151183507258855, 0.003007534715921581642, 0.004007918248335903995 ),
 .UNSPECIFIED. ) ;
#31220=ORIENTED_EDGE ( 'NONE', *, *, #71850, .T. ) ;
#31223=AXIS2_PLACEMENT_3D ( 'NONE', #67001, #22279, #48154 ) ;
#31226=CARTESIAN_POINT ( 'NONE',  ( 16.30764028314251846, 13.22082560946828522, -1.500000000000002220 ) ) ;
#31228=CARTESIAN_POINT ( 'NONE',  ( -37.62287095715005592, -24.64965695001467694, 8.947790433994187609 ) ) ;
#31234=CARTESIAN_POINT ( 'NONE',  ( -79.62287095715005592, -23.47593901973091235, -1.443836447539004642 ) ) ;
#31235=CARTESIAN_POINT ( 'NONE',  ( -0.8134642310582372859, 22.17477653155656725, 11.49999999999999645 ) ) ;
#31237=CARTESIAN_POINT ( 'NONE',  ( -38.52287095715008292, -23.48783264083452593, -1.443836473374935592 ) ) ;
#31238=CARTESIAN_POINT ( 'NONE',  ( -74.52287095715007581, -23.47596703998600631, 11.44779298504228748 ) ) ;
#31239=ORIENTED_EDGE ( 'NONE', *, *, #34911, .F. ) ;
#31240=CARTESIAN_POINT ( 'NONE',  ( 22.15051849217804403, -4.756829024181505439, 11.49999999999998934 ) ) ;
#31244=CARTESIAN_POINT ( 'NONE',  ( -113.2228709571500644, -23.47596703998600631, 11.44779298504227860 ) ) ;
#31246=CARTESIAN_POINT ( 'NONE',  ( -15.35229381799144299, -13.07563953244551591, 11.49999999999998934 ) ) ;
#31247=CARTESIAN_POINT ( 'NONE',  ( -81.62287095715005592, -24.35013146730203459, 9.818937971375111928 ) ) ;
#31248=VERTEX_POINT ( 'NONE', #31909 ) ;
#31249=CARTESIAN_POINT ( 'NONE',  ( -94.62287095715005592, -29.50250243563736774, 8.947779886222139822 ) ) ;
#31250=CARTESIAN_POINT ( 'NONE',  ( -19.39139147909919458, -11.06001032434818576, -1.500000000000002220 ) ) ;
#31251=EDGE_LOOP ( 'NONE', ( #65998, #96728, #49090, #22694 ) ) ;
#31253=CARTESIAN_POINT ( 'NONE',  ( -101.4413695709857990, -25.25341166521219805, 6.524206359329101090 ) ) ;
#31255=CARTESIAN_POINT ( 'NONE',  ( -69.34303308397305443, -25.24554880456021522, 6.209207408033732278 ) ) ;
#31258=CARTESIAN_POINT ( 'NONE',  ( -30.62207085380013183, -24.04615231314291179, -0.4716817114508918829 ) ) ;
#31260=CARTESIAN_POINT ( 'NONE',  ( 10.86043079284791091, -16.25897383129715834, 11.49999999999998934 ) ) ;
#31262=LINE ( 'NONE', #16030, #86298 ) ;
#31263=CARTESIAN_POINT ( 'NONE',  ( 20.96596170256846747, -4.772324250704091497, 11.49999999999998934 ) ) ;
#31264=CARTESIAN_POINT ( 'NONE',  ( -128.5222656252491902, -23.48783264082478794, -1.443836473390056829 ) ) ;
#31265=CARTESIAN_POINT ( 'NONE',  ( -51.52287095715006870, -24.65952944569304606, 1.056160979905693686 ) ) ;
#31266=CARTESIAN_POINT ( 'NONE',  ( -71.55620429048337883, -23.48786465467241058, 11.44779295918254292 ) ) ;
#31267=EDGE_CURVE ( 'NONE', #14750, #34120, #24294, .T. ) ;
#31268=CARTESIAN_POINT ( 'NONE',  ( -80.62287095715007013, -23.47596703998600631, 11.44779298504227860 ) ) ;
#31269=CARTESIAN_POINT ( 'NONE',  ( 15.09361930729867574, -17.17024899132524496, -1.500000000000002220 ) ) ;
#31271=CARTESIAN_POINT ( 'NONE',  ( -96.51331733479386799, -24.15620529776628445, 10.23563542870660115 ) ) ;
#31272=CARTESIAN_POINT ( 'NONE',  ( -53.65874886358959373, -23.48783264082475952, -1.443836473390095909 ) ) ;
#31273=CARTESIAN_POINT ( 'NONE',  ( 1.468936567494551593, -19.95401460376903913, 11.49999999999999645 ) ) ;
#31274=FACE_OUTER_BOUND ( 'NONE', #31107, .T. ) ;
#31275=DIRECTION ( 'NONE',  ( -3.773278334444166432E-23, 1.000000000000000000, 0.000000000000000000 ) ) ;
#31278=VERTEX_POINT ( 'NONE', #48654 ) ;
#31280=CARTESIAN_POINT ( 'NONE',  ( -97.62287095715005592, -29.50250243563736774, 8.947779886222138046 ) ) ;
#31281=CARTESIAN_POINT ( 'NONE',  ( 21.72137571921558319, 1.130696696492564213, 11.49999999999998934 ) ) ;
#31282=CARTESIAN_POINT ( 'NONE',  ( -45.52287095715007581, -24.63345952396255001, 9.038047939301508293 ) ) ;
#31283=CARTESIAN_POINT ( 'NONE',  ( -18.74838588596843181, -5.942601993926947657, -1.500000000000002220 ) ) ;
#31285=AXIS2_PLACEMENT_3D ( 'NONE', #20913, #27049, #97052 ) ;
#31286=CARTESIAN_POINT ( 'NONE',  ( -109.3602963299949806, -25.31697955520687771, 4.255031523248292480 ) ) ;
#31289=CARTESIAN_POINT ( 'NONE',  ( -56.62287095715008434, -23.47596703998600276, 11.44779298504227683 ) ) ;
#31291=CARTESIAN_POINT ( 'NONE',  ( 3.086129920417311823, 20.35385046113321295, 11.49999999999999645 ) ) ;
#31292=CARTESIAN_POINT ( 'NONE',  ( -27.70544111104076990, -24.65058036537550024, 8.251826706788236265 ) ) ;
#31293=CARTESIAN_POINT ( 'NONE',  ( -120.5910596545900120, -24.15503026093913874, -0.2815557561904504791 ) ) ;
#31297=CARTESIAN_POINT ( 'NONE',  ( -46.62287095715006302, -24.34917612406838217, 0.1852690917426625117 ) ) ;
#31298=CARTESIAN_POINT ( 'NONE',  ( -39.61224275064198963, -25.18430957889518496, 3.692191345043688511 ) ) ;
#31299=CARTESIAN_POINT ( 'NONE',  ( -97.59977826141401636, -23.48783264082477018, -1.443836473390088360 ) ) ;
#31302=B_SPLINE_CURVE_WITH_KNOTS ( 'NONE', 3,
 ( #89927, #59481, #66123, #42287, #27538, #43757 ),
 .UNSPECIFIED., .F., .F.,
 ( 4, 2, 4 ),
 ( 0.000000000000000000, 0.001380901958385396351, 0.002761803916770792702 ),
 .UNSPECIFIED. ) ;
#31305=CARTESIAN_POINT ( 'NONE',  ( 22.18053613645642841, 6.281410551025238043, 11.49999999999999645 ) ) ;
#31306=CARTESIAN_POINT ( 'NONE',  ( 15.15630024635751383, 17.02982414992789018, 11.49999999999998934 ) ) ;
#31307=CARTESIAN_POINT ( 'NONE',  ( -74.54565784544875839, -24.34968618360933590, 0.1864209137778816416 ) ) ;
#31308=B_SPLINE_SURFACE_WITH_KNOTS ( 'NONE', 3, 1, ( 
 ( #46530, #23675 ),
 ( #17072, #40421 ),
 ( #15568, #100282 ),
 ( #56158, #54650 ),
 ( #85582, #16064 ),
 ( #69364, #47037 ),
 ( #87086, #79475 ),
 ( #16564, #39911 ),
 ( #47538, #30803 ),
 ( #38411, #77953 ),
 ( #1367, #63275 ),
 ( #92687, #8466 ),
 ( #39417, #853 ),
 ( #31807, #24676 ),
 ( #349, #77458 ) ),
 .UNSPECIFIED., .F., .F., .F.,
 ( 4, 1, 1, 1, 1, 1, 1, 1, 1, 1, 1, 1, 4 ),
 ( 2, 2 ),
 ( 0.000000000000000000, 0.1101655532114483721, 0.2157872561749787366, 0.3180274349094209807, 0.4175739541655078546, 0.5116504876474516905, 0.5961620971027632443, 0.6729345334849961002, 0.7436695573498580680, 0.8106770010653628900, 0.8740589623137356989, 0.9366963019193721429, 1.000000000000000000 ),
 ( 0.000000000000000000, 1.000000000000000000 ),
 .UNSPECIFIED. ) ;
#31309=CARTESIAN_POINT ( 'NONE',  ( -96.60008298486154388, -23.48783264082477018, -1.443836473390089914 ) ) ;
#31311=CARTESIAN_POINT ( 'NONE',  ( -8.193370562272118462, -20.86776251599019361, 11.49999999999999645 ) ) ;
#31312=VERTEX_POINT ( 'NONE', #55260 ) ;
#31313=CARTESIAN_POINT ( 'NONE',  ( -64.52287095715006160, -29.50248528299804818, 1.056150453629034924 ) ) ;
#31314=CARTESIAN_POINT ( 'NONE',  ( -72.62287095715005592, -29.50248528299804818, 1.056150453629036701 ) ) ;
#31315=CARTESIAN_POINT ( 'NONE',  ( -20.07106029494397248, -8.819774368769808248, 11.49999999999998934 ) ) ;
#31317=CARTESIAN_POINT ( 'NONE',  ( -44.52975563414968008, -24.66019654487199020, 8.947790411086115725 ) ) ;
#31318=CARTESIAN_POINT ( 'NONE',  ( -69.07358128771278416, -25.17156706459151394, 6.804697550444784859 ) ) ;
#31320=LINE ( 'NONE', #45562, #84849 ) ;
#31323=EDGE_CURVE ( 'NONE', #80599, #69536, #91780, .T. ) ;
#31324=CARTESIAN_POINT ( 'NONE',  ( 8.813945691637787405, 18.49579627399651471, -1.500000000000002220 ) ) ;
#31325=VERTEX_POINT ( 'NONE', #16674 ) ;
#31329=CARTESIAN_POINT ( 'NONE',  ( -13.34915495237762251, 18.83725853537101358, -1.500000000000002220 ) ) ;
#31330=CARTESIAN_POINT ( 'NONE',  ( -49.15015151476772814, -25.24433540152454825, 3.685374804461877929 ) ) ;
#31331=CARTESIAN_POINT ( 'NONE',  ( -8.348131891436525009, -18.51812344263101906, -1.500000000000002220 ) ) ;
#31335=DIRECTION ( 'NONE',  ( 0.000000000000000000, -2.173523156925980399E-06, 0.9999999999976378895 ) ) ;
#31336=CARTESIAN_POINT ( 'NONE',  ( -87.62287095715004170, -29.50247984919015209, -1.443849546365051806 ) ) ;
#31337=ADVANCED_FACE ( 'NONE', ( #32913 ), #49927, .T. ) ;
#31338=PLANE ( 'NONE',  #36710 ) ;
#31340=CARTESIAN_POINT ( 'NONE',  ( 15.57385778016992894, -14.83193121981731544, 11.49999999999999645 ) ) ;
#31341=ORIENTED_EDGE ( 'NONE', *, *, #67338, .T. ) ;
#31342=CARTESIAN_POINT ( 'NONE',  ( -75.64825452142250128, -23.85016227208580730, -0.8807180028928284221 ) ) ;
#31347=EDGE_CURVE ( 'NONE', #59306, #27806, #50647, .T. ) ;
#31348=CARTESIAN_POINT ( 'NONE',  ( 20.09396958936853395, 5.161349618257207617, 11.49999999999998934 ) ) ;
#31349=VERTEX_POINT ( 'NONE', #33908 ) ;
#31351=ORIENTED_EDGE ( 'NONE', *, *, #21976, .T. ) ;
#31352=CARTESIAN_POINT ( 'NONE',  ( -111.5135283796893617, -24.66019654487200441, 8.947790411086105067 ) ) ;
#31353=CARTESIAN_POINT ( 'NONE',  ( -61.52287095715006160, -24.65952944569304606, 1.056160979905695463 ) ) ;
#31354=ORIENTED_EDGE ( 'NONE', *, *, #14486, .F. ) ;
#31355=ORIENTED_EDGE ( 'NONE', *, *, #60694, .T. ) ;
#31359=CARTESIAN_POINT ( 'NONE',  ( -102.5228709571500332, -24.33927499327854349, 9.819080762295810061 ) ) ;
#31360=CARTESIAN_POINT ( 'NONE',  ( 21.66556372666567754, 3.824538051775513647, 11.49999999999999645 ) ) ;
#31361=CARTESIAN_POINT ( 'NONE',  ( -89.58845897716231832, -24.35071581493543391, 9.817618358456025263 ) ) ;
#31362=CARTESIAN_POINT ( 'NONE',  ( 13.09772080625096891, 18.35129493929886380, -1.500000000000002220 ) ) ;
#31363=CARTESIAN_POINT ( 'NONE',  ( 18.89479412359299815, 9.153864009170110450, 11.49999999999998934 ) ) ;
#31364=VECTOR ( 'NONE', #97321, 1000.000000000000114 ) ;
#31367=ORIENTED_EDGE ( 'NONE', *, *, #57176, .F. ) ;
#31370=B_SPLINE_CURVE_WITH_KNOTS ( 'NONE', 3,
 ( #83069, #98804, #53153, #74961 ),
 .UNSPECIFIED., .F., .F.,
 ( 4, 4 ),
 ( 0.000000000000000000, 9.999999999999592548E-05 ),
 .UNSPECIFIED. ) ;
#31371=LINE ( 'NONE', #8030, #86229 ) ;
#31373=CARTESIAN_POINT ( 'NONE',  ( 20.98173926746349238, 2.650078317256617577, 11.49999999999998934 ) ) ;
#31375=CARTESIAN_POINT ( 'NONE',  ( -61.66187308073543250, -25.27183489919806192, 3.712349809207165841 ) ) ;
#31376=CARTESIAN_POINT ( 'NONE',  ( -121.5883704999377102, -24.65952944569305316, 1.056160979905707897 ) ) ;
#31377=CARTESIAN_POINT ( 'NONE',  ( -94.52287095715006160, -23.47596703998600631, 11.44779298504228393 ) ) ;
#31378=CARTESIAN_POINT ( 'NONE',  ( -127.5228709571500616, -24.35013146730204525, 9.818937971375092388 ) ) ;
#31379=B_SPLINE_CURVE_WITH_KNOTS ( 'NONE', 3,
 ( #30064, #28579, #90479, #37684 ),
 .UNSPECIFIED., .F., .F.,
 ( 4, 4 ),
 ( 0.8310934634990968517, 0.8400998947712122744 ),
 .UNSPECIFIED. ) ;
#31380=CARTESIAN_POINT ( 'NONE',  ( 13.47465251475156656, -17.59220275312388182, -1.500000000000002220 ) ) ;
#31381=VECTOR ( 'NONE', #61097, 1000.000000000000114 ) ;
#31383=EDGE_CURVE ( 'NONE', #65831, #87201, #45780, .T. ) ;
#31387=CARTESIAN_POINT ( 'NONE',  ( -43.62287095715004881, -23.48783264082477729, -1.443836473390071928 ) ) ;
#31388=EDGE_CURVE ( 'NONE', #65697, #22696, #4633, .T. ) ;
#31389=CARTESIAN_POINT ( 'NONE',  ( -100.6244608836033336, -24.92564183028979130, 1.928384488918251760 ) ) ;
#31390=CARTESIAN_POINT ( 'NONE',  ( -34.62287095715005592, -29.50250243563736774, 8.947779886222150481 ) ) ;
#31391=CARTESIAN_POINT ( 'NONE',  ( 19.33761327413411024, 2.027444641817329973, 11.49999999999998934 ) ) ;
#31392=CARTESIAN_POINT ( 'NONE',  ( -13.99230614532761052, -16.21612836239924960, 11.49999999999998934 ) ) ;
#31393=CARTESIAN_POINT ( 'NONE',  ( -62.54344358126193271, -24.34968618360933945, 0.1864209137778798930 ) ) ;
#31394=CARTESIAN_POINT ( 'NONE',  ( -60.49077534611401319, -24.63419186845290199, 9.035850630957110496 ) ) ;
#31396=CARTESIAN_POINT ( 'NONE',  ( -101.0406423489954477, -25.27360018180653967, 3.494480365757756779 ) ) ;
#31397=CARTESIAN_POINT ( 'NONE',  ( -5.793434319722853054, -21.96748078227757617, -1.500000000000002220 ) ) ;
#31398=B_SPLINE_SURFACE_WITH_KNOTS ( 'NONE', 3, 1, ( 
 ( #30844, #49089 ),
 ( #80019, #57210 ),
 ( #80520, #18123 ),
 ( #56708, #25227 ),
 ( #64835, #26237 ),
 ( #2409, #10007 ),
 ( #11012, #47585 ),
 ( #18612, #86631 ),
 ( #72921, #56205 ),
 ( #87131, #95746 ),
 ( #10504, #40965 ) ),
 .UNSPECIFIED., .F., .F., .F.,
 ( 4, 1, 1, 1, 1, 1, 1, 1, 4 ),
 ( 2, 2 ),
 ( 0.000000000000000000, 0.1219040408698844752, 0.2394126076020045568, 0.3554101042801769972, 0.4720907288033014959, 0.5928589821563612361, 0.7187034677136832084, 0.8548923829515286954, 0.9999999999999998890 ),
 ( 0.000000000000000000, 1.000000000000000000 ),
 .UNSPECIFIED. ) ;
#31399=EDGE_CURVE ( 'NONE', #19500, #30802, #22761, .T. ) ;
#31402=CARTESIAN_POINT ( 'NONE',  ( 16.46483878678964174, 11.07114234313464252, 11.49999999999999645 ) ) ;
#31404=CARTESIAN_POINT ( 'NONE',  ( -31.52287095715006160, -23.47593901973090169, -1.443836447538997536 ) ) ;
#31405=ORIENTED_EDGE ( 'NONE', *, *, #41131, .F. ) ;
#31407=ADVANCED_FACE ( 'NONE', ( #19169 ), #74461, .F. ) ;
#31408=CARTESIAN_POINT ( 'NONE',  ( -80.52287095715007581, -24.91570333825475458, 8.075032458260915647 ) ) ;
#31409=VECTOR ( 'NONE', #16086, 1000.000000000000114 ) ;
#31411=CARTESIAN_POINT ( 'NONE',  ( -10.14273968512601520, 19.10955606681249463, -1.500000000000002220 ) ) ;
#31412=CARTESIAN_POINT ( 'NONE',  ( -29.62287096154833677, -23.39681786206389447, 11.44779298504227860 ) ) ;
#31413=CARTESIAN_POINT ( 'NONE',  ( -14.39514105012195344, 13.04300321504834947, -1.500000000000002220 ) ) ;
#31414=CARTESIAN_POINT ( 'NONE',  ( -55.59257803871130932, -24.40133493613049964, 9.663955038902800609 ) ) ;
#31415=CARTESIAN_POINT ( 'NONE',  ( 17.96171645398845129, 8.431260308876343146, 11.49999999999998934 ) ) ;
#31417=AXIS2_PLACEMENT_3D ( 'NONE', #39441, #40942, #41444 ) ;
#31418=CARTESIAN_POINT ( 'NONE',  ( -2.125485521908593078, 20.27274140177646444, 11.49999999999999645 ) ) ;
#31419=CARTESIAN_POINT ( 'NONE',  ( -80.55868892812124216, -23.85016227208580730, -0.8807180028928341953 ) ) ;
#31421=CARTESIAN_POINT ( 'NONE',  ( -123.5228709571500616, -29.50250243563736774, 8.947779886222134493 ) ) ;
#31422=EDGE_LOOP ( 'NONE', ( #79687, #77108, #89343, #16258 ) ) ;
#31423=CARTESIAN_POINT ( 'NONE',  ( -41.41113444086114725, -25.26397904058624277, 3.881650733674827602 ) ) ;
#31424=CARTESIAN_POINT ( 'NONE',  ( -92.52287095715007581, -24.50216790748206108, 0.6166512839542513946 ) ) ;
#31427=DIRECTION ( 'NONE',  ( -3.773278334453079618E-23, 0.9999999999976377785, 2.173523156925979975E-06 ) ) ;
#31428=CARTESIAN_POINT ( 'NONE',  ( 17.00595499256408871, 10.69956108467327205, 11.49999999999998934 ) ) ;
#31429=AXIS2_PLACEMENT_3D ( 'NONE', #41442, #73886, #19588 ) ;
#31430=DIRECTION ( 'NONE',  ( 3.773278334444167608E-23, -1.000000000000000000, 0.000000000000000000 ) ) ;
#31431=ORIENTED_EDGE ( 'NONE', *, *, #60898, .T. ) ;
#31433=CARTESIAN_POINT ( 'NONE',  ( -22.32109313027335062, -5.015931025267754251, 11.49999999999999645 ) ) ;
#31434=CARTESIAN_POINT ( 'NONE',  ( -20.26579564662877075, -10.28286414166031726, -1.500000000000002220 ) ) ;
#31436=CARTESIAN_POINT ( 'NONE',  ( -71.70011599639640565, -25.23854420923243325, 6.372362213873513426 ) ) ;
#31439=CARTESIAN_POINT ( 'NONE',  ( -30.57287095715006231, -24.49177996402112356, 9.428047631786927951 ) ) ;
#31440=CARTESIAN_POINT ( 'NONE',  ( -128.5218873095093954, -23.96169478059714919, 10.65365249895717170 ) ) ;
#31442=ORIENTED_EDGE ( 'NONE', *, *, #59294, .T. ) ;
#31443=CARTESIAN_POINT ( 'NONE',  ( 16.53694760393551988, -11.94906295602464397, 11.49999999999998934 ) ) ;
#31445=EDGE_CURVE ( 'NONE', #19525, #16750, #88219, .T. ) ;
#31446=B_SPLINE_CURVE_WITH_KNOTS ( 'NONE', 3,
 ( #88821, #18791, #11188, #80200 ),
 .UNSPECIFIED., .F., .F.,
 ( 4, 4 ),
 ( 0.000000000000000000, 1.000000000000000000 ),
 .UNSPECIFIED. ) ;
#31447=CARTESIAN_POINT ( 'NONE',  ( -14.90462150274475306, 17.49973755783957685, 11.49999999999998934 ) ) ;
#31448=CARTESIAN_POINT ( 'NONE',  ( -54.49167730237748231, -24.51419770103157347, 9.386484678747178734 ) ) ;
#31449=ORIENTED_EDGE ( 'NONE', *, *, #98274, .T. ) ;
#31450=CARTESIAN_POINT ( 'NONE',  ( -101.6228709571500843, -24.50321055353805377, 9.387540953477515160 ) ) ;
#31451=CARTESIAN_POINT ( 'NONE',  ( -81.04628668253678825, -25.15830465083685752, 6.953829097328267927 ) ) ;
#31452=CARTESIAN_POINT ( 'NONE',  ( -96.62287095715005592, -23.47593901973091235, -1.443836447539001089 ) ) ;
#31453=CARTESIAN_POINT ( 'NONE',  ( 7.794017451908327843, -19.83292067980804774, 11.49999999999999645 ) ) ;
#31454=ORIENTED_EDGE ( 'NONE', *, *, #90920, .T. ) ;
#31455=B_SPLINE_CURVE_WITH_KNOTS ( 'NONE', 3,
 ( #55030, #46912, #9843, #2248 ),
 .UNSPECIFIED., .F., .F.,
 ( 4, 4 ),
 ( 0.000000000000000000, 9.999999999998897304E-05 ),
 .UNSPECIFIED. ) ;
#31457=ORIENTED_EDGE ( 'NONE', *, *, #32717, .T. ) ;
#31458=CARTESIAN_POINT ( 'NONE',  ( 9.120982285578694615, 20.23247719416018242, -1.500000000000002220 ) ) ;
#31460=CARTESIAN_POINT ( 'NONE',  ( 16.46467569749531634, 12.45148609503053017, -1.500000000000002220 ) ) ;
#31461=VECTOR ( 'NONE', #70103, 1000.000000000000114 ) ;
#31462=ORIENTED_EDGE ( 'NONE', *, *, #21004, .F. ) ;
#31463=ORIENTED_EDGE ( 'NONE', *, *, #16553, .T. ) ;
#31464=CARTESIAN_POINT ( 'NONE',  ( -112.6228709571500701, -24.50321055353806443, 9.387540953477524042 ) ) ;
#31465=CARTESIAN_POINT ( 'NONE',  ( -95.63923326134215586, -23.85049219812686161, 10.88485053497527133 ) ) ;
#31467=CARTESIAN_POINT ( 'NONE',  ( -50.12942939268734932, -25.13686567213617806, 7.080268837617579969 ) ) ;
#31469=CARTESIAN_POINT ( 'NONE',  ( -58.58292334261074075, -24.51419770103156637, 9.386484678747176957 ) ) ;
#31471=CARTESIAN_POINT ( 'NONE',  ( -15.88994834598175387, -13.44966708658631838, -1.500000000000002220 ) ) ;
#31473=CARTESIAN_POINT ( 'NONE',  ( 21.07893183998518438, -5.767110019903106455, 11.49999999999999645 ) ) ;
#31475=FACE_OUTER_BOUND ( 'NONE', #84406, .T. ) ;
#31476=CARTESIAN_POINT ( 'NONE',  ( -78.62361342553873556, -24.66019654487200441, 8.947790411086119278 ) ) ;
#31477=CARTESIAN_POINT ( 'NONE',  ( -21.16806448877717628, 7.570426553894726851, -1.500000000000002220 ) ) ;
#31478=CARTESIAN_POINT ( 'NONE',  ( -118.6235039397453335, -24.66019654487199730, 8.947790411086115725 ) ) ;
#31479=DIRECTION ( 'NONE',  ( 0.000000000000000000, 0.9999999999976377785, 2.173523156925979975E-06 ) ) ;
#31481=ORIENTED_EDGE ( 'NONE', *, *, #24819, .T. ) ;
#31482=ORIENTED_EDGE ( 'NONE', *, *, #97660, .T. ) ;
#31484=CARTESIAN_POINT ( 'NONE',  ( -11.21157863559261791, -18.18922556752850994, -1.500000000000002220 ) ) ;
#31485=VERTEX_POINT ( 'NONE', #53138 ) ;
#31486=CARTESIAN_POINT ( 'NONE',  ( 19.40125262130244366, -8.172613994405130811, 11.49999999999998934 ) ) ;
#31487=CARTESIAN_POINT ( 'NONE',  ( -30.43724401707702754, -24.37552172231524494, 0.3015907515355735202 ) ) ;
#31488=CARTESIAN_POINT ( 'NONE',  ( 6.088051586893210576, -19.00464151315268424, -1.500000000000002220 ) ) ;
#31489=CARTESIAN_POINT ( 'NONE',  ( -50.47720752119995780, -24.92592662359561473, 8.075495903018000021 ) ) ;
#31491=CARTESIAN_POINT ( 'NONE',  ( 5.346615758220810477, 21.33151429383102382, -1.500000000000002220 ) ) ;
#31492=DIRECTION ( 'NONE',  ( 0.000000000000000000, -2.173523156925979552E-06, 0.9999999999976378895 ) ) ;
#31496=CARTESIAN_POINT ( 'NONE',  ( -20.80165436122882383, -1.723964017131293103, 11.49999999999999645 ) ) ;
#31500=AXIS2_PLACEMENT_3D ( 'NONE', #10070, #8576, #48656 ) ;
#31501=CARTESIAN_POINT ( 'NONE',  ( -38.62287095715005592, -24.66019654487199020, 8.947790411086137041 ) ) ;
#31502=CARTESIAN_POINT ( 'NONE',  ( 21.17668642892995834, 2.279540523802085605, -1.500000000000002220 ) ) ;
#31503=CARTESIAN_POINT ( 'NONE',  ( -46.62287095715004881, -23.48786465467241058, 11.44779295918255180 ) ) ;
#31505=B_SPLINE_CURVE_WITH_KNOTS ( 'NONE', 3,
 ( #41548, #64408, #48674, #43423 ),
 .UNSPECIFIED., .F., .F.,
 ( 4, 4 ),
 ( 0.8110791717832845915, 0.8200856030554002363 ),
 .UNSPECIFIED. ) ;
#31508=CARTESIAN_POINT ( 'NONE',  ( -12.86601690267178100, 18.50254183665605012, -1.500000000000002220 ) ) ;
#31509=EDGE_CURVE ( 'NONE', #81354, #73682, #34826, .T. ) ;
#31510=CARTESIAN_POINT ( 'NONE',  ( -129.5228709571500758, -24.65952944569305316, 1.056160979905707675 ) ) ;
#31512=CARTESIAN_POINT ( 'NONE',  ( -79.26673083468246261, -25.30578403561748146, 5.000323484767054794 ) ) ;
#31514=CARTESIAN_POINT ( 'NONE',  ( -5.312243195520525596, -18.98051080891723430, 11.49999999999999645 ) ) ;
#31515=CARTESIAN_POINT ( 'NONE',  ( -125.6228709571500275, -23.48783264082479505, -1.443836473390057273 ) ) ;
#31516=CARTESIAN_POINT ( 'NONE',  ( -32.52287095715005449, -23.73934037231756022, 11.05740245334329686 ) ) ;
#31518=CARTESIAN_POINT ( 'NONE',  ( -99.58877505434060140, -24.34968618360934300, 0.1864209137778966852 ) ) ;
#31520=CARTESIAN_POINT ( 'NONE',  ( -90.93265888899549054, -25.30572777988224331, 5.920366768842380445 ) ) ;
#31521=DIRECTION ( 'NONE',  ( 1.000000000000000000, 3.773278334444166432E-23, 8.201307841325785021E-29 ) ) ;
#31522=CARTESIAN_POINT ( 'NONE',  ( 11.81298147481671279, -15.83112273922526470, -1.500000000000002220 ) ) ;
#31523=VERTEX_POINT ( 'NONE', #84064 ) ;
#31524=CARTESIAN_POINT ( 'NONE',  ( -120.5228709571500048, -24.52323809116984066, 9.355190652339418378 ) ) ;
#31525=AXIS2_PLACEMENT_3D ( 'NONE', #25689, #18078, #67630 ) ;
#31528=VERTEX_POINT ( 'NONE', #29783 ) ;
#31529=CARTESIAN_POINT ( 'NONE',  ( -109.6228709571500275, -23.73934037231757799, 11.05740245334328087 ) ) ;
#31530=DIRECTION ( 'NONE',  ( -1.000000000000000000, -3.773278334444167608E-23, -8.201307833595939069E-29 ) ) ;
#31531=CARTESIAN_POINT ( 'NONE',  ( -100.6183367005896514, -25.30264758658750779, 4.735178788106561676 ) ) ;
#31532=CARTESIAN_POINT ( 'NONE',  ( -99.65618967412262919, -25.26638501296867645, 7.377943290858292258 ) ) ;
#31533=CARTESIAN_POINT ( 'NONE',  ( -67.62287095715008434, -24.33832256526968507, 0.1851278514119886476 ) ) ;
#31534=CARTESIAN_POINT ( 'NONE',  ( -59.52287095715009002, -23.47593901973090524, -1.443836447538997092 ) ) ;
#31535=FACE_OUTER_BOUND ( 'NONE', #54481, .T. ) ;
#31536=CARTESIAN_POINT ( 'NONE',  ( 18.80801646011137507, -6.797914457553222434, -1.500000000000002220 ) ) ;
#31538=CARTESIAN_POINT ( 'NONE',  ( -99.29064586046420970, -25.27532990705892146, 3.426410652678359092 ) ) ;
#31539=FACE_OUTER_BOUND ( 'NONE', #85213, .T. ) ;
#31541=EDGE_CURVE ( 'NONE', #58944, #76875, #8221, .T. ) ;
#31542=ADVANCED_FACE ( 'NONE', ( #46020 ), #76440, .T. ) ;
#31543=B_SPLINE_CURVE_WITH_KNOTS ( 'NONE', 3,
 ( #14906, #47378, #23007, #84925 ),
 .UNSPECIFIED., .F., .F.,
 ( 4, 4 ),
 ( 0.000000000000000000, 9.999999999998897304E-05 ),
 .UNSPECIFIED. ) ;
#31544=ADVANCED_FACE ( 'NONE', ( #44011 ), #76938, .T. ) ;
#31546=CARTESIAN_POINT ( 'NONE',  ( -109.4273347235498193, -25.29012848027490179, 3.857971622509586584 ) ) ;
#31547=CARTESIAN_POINT ( 'NONE',  ( -120.6228709571500417, -23.48783264082479505, -1.443836473390058384 ) ) ;
#31548=CARTESIAN_POINT ( 'NONE',  ( -100.5228709571501042, -24.83620972994592790, 8.398175272781370992 ) ) ;
#31554=CARTESIAN_POINT ( 'NONE',  ( 18.81862293822770837, 7.596102252255398035, 11.49999999999998934 ) ) ;
#31555=B_SPLINE_CURVE_WITH_KNOTS ( 'NONE', 3,
 ( #18141, #70941, #72941, #2427, #17642, #79032, #71441, #78522 ),
 .UNSPECIFIED., .F., .F.,
 ( 4, 2, 2, 4 ),
 ( 0.000000000000000000, 0.002001098010032690590, 0.003001647015049033716, 0.004002196020065376843 ),
 .UNSPECIFIED. ) ;
#31556=B_SPLINE_CURVE_WITH_KNOTS ( 'NONE', 3,
 ( #84006, #99709, #14492, #37838 ),
 .UNSPECIFIED., .F., .F.,
 ( 4, 4 ),
 ( 0.000000000000000000, 9.999999999998897304E-05 ),
 .UNSPECIFIED. ) ;
#31558=CARTESIAN_POINT ( 'NONE',  ( -73.62287095715005592, -23.48786465467241058, 11.44779295918254469 ) ) ;
#31559=CARTESIAN_POINT ( 'NONE',  ( -99.62287095715002749, -23.94994826722516379, -0.6494450866351717533 ) ) ;
#31560=EDGE_LOOP ( 'NONE', ( #93271, #80593, #98335, #10288 ) ) ;
#31562=CARTESIAN_POINT ( 'NONE',  ( -18.49208213979201076, -7.923680710433813168, -1.500000000000002220 ) ) ;
#31563=CARTESIAN_POINT ( 'NONE',  ( 21.03498508994548999, -2.205306954651367946, 11.49999999999999645 ) ) ;
#31565=CARTESIAN_POINT ( 'NONE',  ( -8.904070064990065703, -20.24664451029508783, 11.49999999999998934 ) ) ;
#31567=CARTESIAN_POINT ( 'NONE',  ( 4.814550503181614260, -19.98661186389175271, 11.49999999999998934 ) ) ;
#31568=CARTESIAN_POINT ( 'NONE',  ( -60.59240994803741387, -24.40034930558990922, 0.3402023900116026289 ) ) ;
#31569=ORIENTED_EDGE ( 'NONE', *, *, #62047, .T. ) ;
#31570=FACE_OUTER_BOUND ( 'NONE', #45678, .T. ) ;
#31574=CARTESIAN_POINT ( 'NONE',  ( -80.58953762381672448, -23.47593901973091235, -1.443836447539004642 ) ) ;
#31575=EDGE_LOOP ( 'NONE', ( #53795, #49288, #6355, #85506 ) ) ;
#31576=ORIENTED_EDGE ( 'NONE', *, *, #32563, .T. ) ;
#31577=ORIENTED_EDGE ( 'NONE', *, *, #65723, .T. ) ;
#31578=CARTESIAN_POINT ( 'NONE',  ( -98.52287095715006160, -23.48783264082477018, -1.443836473390087916 ) ) ;
#31579=CARTESIAN_POINT ( 'NONE',  ( -49.96261679139975342, -25.04210150420108505, 7.519895067019000123 ) ) ;
#31580=CARTESIAN_POINT ( 'NONE',  ( -68.58035869059457923, -24.66019654487199375, 8.947790411086122830 ) ) ;
#31581=CARTESIAN_POINT ( 'NONE',  ( -7.658335995763069448, 19.15843701367676388, -1.500000000000002220 ) ) ;
#31583=CARTESIAN_POINT ( 'NONE',  ( 21.52761780497506905, -1.784033869580059939, 11.49999999999999645 ) ) ;
#31585=CARTESIAN_POINT ( 'NONE',  ( -107.5228709571500758, -29.50248528299804818, 1.056150453629043584 ) ) ;
#31587=CARTESIAN_POINT ( 'NONE',  ( -22.19192207843486386, -2.872123673023632584, 11.49999999999998934 ) ) ;
#31588=ADVANCED_FACE ( 'NONE', ( #85061 ), #83053, .T. ) ;
#31589=CARTESIAN_POINT ( 'NONE',  ( -47.66152167227360081, -23.48786465467240347, 11.44779295918255002 ) ) ;
#31592=CARTESIAN_POINT ( 'NONE',  ( -119.4335848664117634, -25.40066263013008196, 5.394419962397462243 ) ) ;
#31593=CARTESIAN_POINT ( 'NONE',  ( -120.6228709571501270, -24.83620972994592435, 8.398175272781365663 ) ) ;
#31594=CARTESIAN_POINT ( 'NONE',  ( -18.74228827200876779, -9.293929619069025705, 11.49999999999998934 ) ) ;
#31598=ORIENTED_EDGE ( 'NONE', *, *, #58263, .F. ) ;
#31599=CARTESIAN_POINT ( 'NONE',  ( -60.62287095715004881, -29.50248528299804818, 1.056150453629034924 ) ) ;
#31600=CARTESIAN_POINT ( 'NONE',  ( -21.05374637409849825, 2.266213160971460194, -1.500000000000002220 ) ) ;
#31602=CARTESIAN_POINT ( 'NONE',  ( -50.58240830060177728, -24.73486907724918282, 1.287355809206965684 ) ) ;
#31603=CARTESIAN_POINT ( 'NONE',  ( -15.04333773895388937, -15.80532200100455498, 11.49999999999998934 ) ) ;
#31605=CARTESIAN_POINT ( 'NONE',  ( -98.62287095715005592, -24.64898659630529210, 1.056161002820829697 ) ) ;
#31606=CARTESIAN_POINT ( 'NONE',  ( -35.52287095715008292, -24.51254535375843702, 9.355368624242190734 ) ) ;
#31607=CARTESIAN_POINT ( 'NONE',  ( -3.204121956075930200, -21.57847171274271858, -1.500000000000002220 ) ) ;
#31608=CARTESIAN_POINT ( 'NONE',  ( -30.57287095715006231, -24.75555062611201507, 1.382286062901152857 ) ) ;
#31609=ORIENTED_EDGE ( 'NONE', *, *, #21109, .T. ) ;
#31617=ORIENTED_EDGE ( 'NONE', *, *, #42264, .T. ) ;
#31618=CARTESIAN_POINT ( 'NONE',  ( -29.16535361088288170, -25.13616264269015232, 3.785723840771683779 ) ) ;
#31620=CARTESIAN_POINT ( 'NONE',  ( 20.41123533131232648, 5.719371238976541427, 11.49999999999998934 ) ) ;
#31621=CARTESIAN_POINT ( 'NONE',  ( -94.54501400172604519, -24.65952944569304606, 1.056160979905701680 ) ) ;
#31622=FACE_BOUND ( 'NONE', #878, .T. ) ;
#31625=CARTESIAN_POINT ( 'NONE',  ( 3.017506814366913481, 19.14668354085002733, 11.49999999999998934 ) ) ;
#31626=EDGE_CURVE ( 'NONE', #9739, #55399, #26379, .T. ) ;
#31627=CARTESIAN_POINT ( 'NONE',  ( -69.37719319406642171, -25.27788132133623833, 5.961564651755576705 ) ) ;
#31629=CARTESIAN_POINT ( 'NONE',  ( -18.23695082634099407, 6.967386181637144738, 11.49999999999999645 ) ) ;
#31630=CARTESIAN_POINT ( 'NONE',  ( -34.55620429048339304, -23.48783264082477729, -1.443836473390074593 ) ) ;
#31633=CARTESIAN_POINT ( 'NONE',  ( -103.5895376238167103, -23.47596703998600631, 11.44779298504227683 ) ) ;
#31634=CARTESIAN_POINT ( 'NONE',  ( -44.52287095715006160, -23.47593901973090169, -1.443836447538997092 ) ) ;
#31635=CARTESIAN_POINT ( 'NONE',  ( -106.5228709571500474, -24.33832256527049154, 0.1851278514138675058 ) ) ;
#31636=CARTESIAN_POINT ( 'NONE',  ( -93.50736637352794389, -24.51419770103157703, 9.386484678747164523 ) ) ;
#31637=CARTESIAN_POINT ( 'NONE',  ( -2.223759785643201869, -19.53228827767608777, 11.49999999999998934 ) ) ;
#31638=CARTESIAN_POINT ( 'NONE',  ( -68.52287095715006160, -24.65952944569304606, 1.056160979905697239 ) ) ;
#31639=ORIENTED_EDGE ( 'NONE', *, *, #53740, .F. ) ;
#31640=B_SPLINE_CURVE_WITH_KNOTS ( 'NONE', 3,
 ( #15665, #14158, #37508, #91781, #90798, #29392 ),
 .UNSPECIFIED., .F., .F.,
 ( 4, 2, 4 ),
 ( 0.000000000000000000, 0.001380764517854769086, 0.002761529035709538171 ),
 .UNSPECIFIED. ) ;
#31642=CARTESIAN_POINT ( 'NONE',  ( 11.83326311654409935, 18.06170320929925310, 11.49999999999998934 ) ) ;
#31643=CARTESIAN_POINT ( 'NONE',  ( -40.47826423538212737, -24.73486907724917927, 1.287355809206960577 ) ) ;
#31644=CARTESIAN_POINT ( 'NONE',  ( -77.62287095715005592, -23.47593901973091235, -1.443836447539004642 ) ) ;
#31645=CARTESIAN_POINT ( 'NONE',  ( 6.910522817300494225, 22.03692736239173300, -1.500000000000002220 ) ) ;
#31648=CARTESIAN_POINT ( 'NONE',  ( -74.52287095715007581, -23.47596703998600631, 11.44779298504228748 ) ) ;
#31649=CARTESIAN_POINT ( 'NONE',  ( -130.5728709571500588, -23.53197991584895021, -1.479945482512685428 ) ) ;
#31650=CARTESIAN_POINT ( 'NONE',  ( -110.6228709571500559, -29.50248789122583659, 2.256150453626215580 ) ) ;
#31651=CARTESIAN_POINT ( 'NONE',  ( -100.4498239493576648, -25.04307398257883932, 7.563174194274490780 ) ) ;
#31653=PLANE ( 'NONE',  #45627 ) ;
#31654=CARTESIAN_POINT ( 'NONE',  ( -99.64934318012689118, -25.26400883459589153, 4.927356406368939901 ) ) ;
#31655=CARTESIAN_POINT ( 'NONE',  ( -19.77041435686880533, -2.435487021107205940, 11.49999999999998934 ) ) ;
#31658=CARTESIAN_POINT ( 'NONE',  ( -7.150643268323968904, -18.52920452239153448, -1.500000000000002220 ) ) ;
#31659=EDGE_CURVE ( 'NONE', #62579, #50327, #17560, .T. ) ;
#31660=FACE_OUTER_BOUND ( 'NONE', #16124, .T. ) ;
#31661=EDGE_CURVE ( 'NONE', #61801, #98189, #32281, .T. ) ;
#31665=CARTESIAN_POINT ( 'NONE',  ( 19.40724743217988291, -7.346346906864608783, 11.49999999999999645 ) ) ;
#31666=CARTESIAN_POINT ( 'NONE',  ( -102.5228709571500758, -23.47596703998600631, 11.44779298504228215 ) ) ;
#31667=VECTOR ( 'NONE', #38263, 1000.000000000000227 ) ;
#31668=CARTESIAN_POINT ( 'NONE',  ( -88.62287095715004170, -23.47593901973091235, -1.443836447539002865 ) ) ;
#31669=CARTESIAN_POINT ( 'NONE',  ( -22.19569011343799048, 5.130922947863589378, 11.49999999999999645 ) ) ;
#31670=VECTOR ( 'NONE', #1880, 1000.000000000000114 ) ;
#31671=VERTEX_POINT ( 'NONE', #63251 ) ;
#31672=CARTESIAN_POINT ( 'NONE',  ( -57.62287095715002749, -24.51283580621364422, 0.6167428607019694864 ) ) ;
#31674=B_SPLINE_CURVE_WITH_KNOTS ( 'NONE', 3,
 ( #96688, #64274, #10451, #25680, #56651, #87588, #72370, #2865 ),
 .UNSPECIFIED., .F., .F.,
 ( 4, 2, 2, 4 ),
 ( -0.001240355328176840580, -0.0002398155169399329104, 0.0007607242942969747596, 0.002761803916770785763 ),
 .UNSPECIFIED. ) ;
#31677=CARTESIAN_POINT ( 'NONE',  ( 2.532258636284850706, -20.04889675553949147, 11.49999999999998934 ) ) ;
#31678=EDGE_CURVE ( 'NONE', #37802, #23353, #17053, .T. ) ;
#31679=EDGE_CURVE ( 'NONE', #81281, #79893, #54629, .T. ) ;
#31682=CARTESIAN_POINT ( 'NONE',  ( -97.62287095715005592, -24.64965695001468404, 8.947790433994178727 ) ) ;
#31683=ORIENTED_EDGE ( 'NONE', *, *, #58385, .T. ) ;
#31686=EDGE_CURVE ( 'NONE', #64811, #37373, #85564, .T. ) ;
#31688=CARTESIAN_POINT ( 'NONE',  ( 18.88093902437788785, 12.95799798663108682, 11.49999999999998934 ) ) ;
#31689=CARTESIAN_POINT ( 'NONE',  ( -51.23509499458276650, -25.27420657037325569, 3.726222110248589292 ) ) ;
#31690=CARTESIAN_POINT ( 'NONE',  ( 21.02075834227166951, -5.193550065563941942, -1.500000000000002220 ) ) ;
#31691=CARTESIAN_POINT ( 'NONE',  ( -104.6228709571500701, -24.51283580621365132, 0.6167428607019816988 ) ) ;
#31692=CARTESIAN_POINT ( 'NONE',  ( 16.15719879640481338, -13.26386290209467944, 11.49999999999999645 ) ) ;
#31693=EDGE_LOOP ( 'NONE', ( #11602, #73940, #39066, #61206 ) ) ;
#31694=DIRECTION ( 'NONE',  ( 3.773278334444166432E-23, -1.000000000000000000, 0.000000000000000000 ) ) ;
#31695=CARTESIAN_POINT ( 'NONE',  ( -68.94292010565295925, -25.24754505917867320, 6.048224126016797264 ) ) ;
#31696=CARTESIAN_POINT ( 'NONE',  ( -21.82725030464235516, 2.967780500094957308, 11.49999999999998934 ) ) ;
#31697=B_SPLINE_CURVE_WITH_KNOTS ( 'NONE', 3,
 ( #48215, #93871, #53824, #24362, #62946, #15244 ),
 .UNSPECIFIED., .F., .F.,
 ( 4, 2, 4 ),
 ( 1.570887131794333942E-05, 0.001396322306279759555, 0.002776935741241575838 ),
 .UNSPECIFIED. ) ;
#31698=EDGE_CURVE ( 'NONE', #99097, #64167, #55416, .T. ) ;
#31699=CARTESIAN_POINT ( 'NONE',  ( -124.4728709548940486, -25.40673988423725049, 2.000950542041663116 ) ) ;
#31701=ORIENTED_EDGE ( 'NONE', *, *, #3975, .F. ) ;
#31702=CARTESIAN_POINT ( 'NONE',  ( -49.63711845704647629, -25.27344830480632609, 3.620155576039564504 ) ) ;
#31703=CARTESIAN_POINT ( 'NONE',  ( -46.58953762381671737, -23.48783264082478439, -1.443836473390070818 ) ) ;
#31707=ORIENTED_EDGE ( 'NONE', *, *, #15618, .F. ) ;
#31708=CARTESIAN_POINT ( 'NONE',  ( -61.64687923781919920, -25.20074463982482982, 3.409327697717700278 ) ) ;
#31709=CARTESIAN_POINT ( 'NONE',  ( -92.52287095715006160, -29.50247984919015209, -1.443849546365051806 ) ) ;
#31711=CARTESIAN_POINT ( 'NONE',  ( 13.99439195134931069, 14.96789054323355828, -1.500000000000002220 ) ) ;
#31712=EDGE_CURVE ( 'NONE', #78336, #71801, #47016, .T. ) ;
#31715=CARTESIAN_POINT ( 'NONE',  ( -44.56898227375175026, -23.48783264082476663, -1.443836473390095021 ) ) ;
#31717=CARTESIAN_POINT ( 'NONE',  ( 21.78807519107708401, 4.755904613692067073, -1.500000000000002220 ) ) ;
#31718=EDGE_CURVE ( 'NONE', #39067, #65225, #6961, .T. ) ;
#31719=CARTESIAN_POINT ( 'NONE',  ( -55.52287095715006870, -24.92604778743017135, 8.074972756849364330 ) ) ;
#31720=CARTESIAN_POINT ( 'NONE',  ( -26.49221882413262819, -24.65723053117703500, 7.825584094027206561 ) ) ;
#31723=CARTESIAN_POINT ( 'NONE',  ( -29.36544338184978642, -24.97648490869306315, 2.618731075491085747 ) ) ;
#31724=CARTESIAN_POINT ( 'NONE',  ( -73.52287095715010423, -23.48783264082477018, -1.443836473390093689 ) ) ;
#31726=CARTESIAN_POINT ( 'NONE',  ( -17.75621389795859884, -10.86975384844714831, 11.49999999999998934 ) ) ;
#31728=CARTESIAN_POINT ( 'NONE',  ( -51.62287095715005592, -24.64898659630367206, 1.056161002820821038 ) ) ;
#31732=CARTESIAN_POINT ( 'NONE',  ( -20.70934228997045068, 3.328930095467914185, -1.500000000000002220 ) ) ;
#31734=CARTESIAN_POINT ( 'NONE',  ( -69.52287095715004739, -24.35013146730203815, 9.818937971375103047 ) ) ;
#31735=CARTESIAN_POINT ( 'NONE',  ( -82.52287095715006160, -23.47593901973090169, -1.443836447538996648 ) ) ;
#31737=FACE_OUTER_BOUND ( 'NONE', #87611, .T. ) ;
#31738=CARTESIAN_POINT ( 'NONE',  ( -59.62366531831469274, -24.65952944569304961, 1.056160979905697905 ) ) ;
#31740=CARTESIAN_POINT ( 'NONE',  ( 21.18294168759468832, 6.642818831845659133, 11.49999999999999645 ) ) ;
#31741=ORIENTED_EDGE ( 'NONE', *, *, #45551, .F. ) ;
#31742=CARTESIAN_POINT ( 'NONE',  ( -108.6228709571500559, -23.47593901973091235, -1.443836447538999312 ) ) ;
#31744=EDGE_LOOP ( 'NONE', ( #18958, #20085, #80815, #82797 ) ) ;
#31745=CARTESIAN_POINT ( 'NONE',  ( 12.64511023617726160, -18.80563239904246231, 11.49999999999998934 ) ) ;
#31746=CARTESIAN_POINT ( 'NONE',  ( -87.52287095715006160, -23.47593901973090524, -1.443836447538996648 ) ) ;
#31747=VERTEX_POINT ( 'NONE', #16542 ) ;
#31748=B_SPLINE_CURVE_WITH_KNOTS ( 'NONE', 3,
 ( #87037, #1813, #89050, #63733 ),
 .UNSPECIFIED., .F., .F.,
 ( 4, 4 ),
 ( 0.4608290667565730359, 0.4698354980286885696 ),
 .UNSPECIFIED. ) ;
#31749=ORIENTED_EDGE ( 'NONE', *, *, #16882, .F. ) ;
#31751=VECTOR ( 'NONE', #79984, 1000.000000000000114 ) ;
#31752=CARTESIAN_POINT ( 'NONE',  ( 7.141438900065890216, -18.84860497471923679, -1.500000000000002220 ) ) ;
#31753=CARTESIAN_POINT ( 'NONE',  ( -80.62287095715005592, -24.15431212366392444, -0.2830839119429126582 ) ) ;
#31757=CARTESIAN_POINT ( 'NONE',  ( -3.217810451210200817, -22.18463865543611391, -1.500000000000002220 ) ) ;
#31762=CARTESIAN_POINT ( 'NONE',  ( -101.5158928754072605, -25.16257325694536817, 6.338294381039898617 ) ) ;
#31764=CARTESIAN_POINT ( 'NONE',  ( -40.35495219140244672, -25.31533539124680487, 5.080713930537138268 ) ) ;
#31767=CARTESIAN_POINT ( 'NONE',  ( -30.60914355658976049, -24.37807914296825729, 0.3010598746230576106 ) ) ;
#31768=CARTESIAN_POINT ( 'NONE',  ( -16.69004703121433408, -10.21020960635683394, -1.500000000000002220 ) ) ;
#31769=CARTESIAN_POINT ( 'NONE',  ( -33.52287095715006160, -24.64898659630367206, 1.056161002820817485 ) ) ;
#31770=ORIENTED_EDGE ( 'NONE', *, *, #54270, .T. ) ;
#31771=CARTESIAN_POINT ( 'NONE',  ( 8.645823604709390153, 19.67543227842514852, -1.500000000000002220 ) ) ;
#31774=CARTESIAN_POINT ( 'NONE',  ( -118.2228709571500787, -23.47593901973090524, -1.443836447538996426 ) ) ;
#31775=CARTESIAN_POINT ( 'NONE',  ( -70.55620429048340725, -25.00182538069145721, 7.747789668545099317 ) ) ;
#31776=CARTESIAN_POINT ( 'NONE',  ( 16.54545882101025711, 15.75737887292823558, -1.500000000000002220 ) ) ;
#31778=CARTESIAN_POINT ( 'NONE',  ( -46.52287095715006160, -24.64898659630367561, 1.056161002820821038 ) ) ;
#31779=CARTESIAN_POINT ( 'NONE',  ( -92.62287095715004170, -23.72747288104469376, -1.053458166803225460 ) ) ;
#31780=CARTESIAN_POINT ( 'NONE',  ( -10.28607412905329532, -17.16720287211733975, 11.49999999999999645 ) ) ;
#31781=CARTESIAN_POINT ( 'NONE',  ( -54.62287095715004881, -23.48783264082478084, -1.443836473390070596 ) ) ;
#31786=B_SPLINE_CURVE_WITH_KNOTS ( 'NONE', 3,
 ( #67500, #28923, #75582, #470 ),
 .UNSPECIFIED., .F., .F.,
 ( 4, 4 ),
 ( 0.000000000000000000, 0.0004038461538461296518 ),
 .UNSPECIFIED. ) ;
#31787=DIRECTION ( 'NONE',  ( -3.773278334453079618E-23, 0.9999999999976377785, 2.173523156925979975E-06 ) ) ;
#31790=CARTESIAN_POINT ( 'NONE',  ( -21.33044368757495590, -4.375833669458513597, 11.49999999999998934 ) ) ;
#31791=CARTESIAN_POINT ( 'NONE',  ( -118.6228709571500559, -29.50248528299804818, 1.056150453629045360 ) ) ;
#31792=CARTESIAN_POINT ( 'NONE',  ( 19.58216393897113505, 1.562425146961006650, -1.500000000000002220 ) ) ;
#31795=CARTESIAN_POINT ( 'NONE',  ( -85.52287095715004739, -23.85229601348995487, 10.88205029486208808 ) ) ;
#31799=CARTESIAN_POINT ( 'NONE',  ( -91.54878298496558386, -24.35071581493543391, 9.817618358456025263 ) ) ;
#31800=CARTESIAN_POINT ( 'NONE',  ( -73.62287095715002749, -24.51387760970725083, 9.387446482453428942 ) ) ;
#31801=CARTESIAN_POINT ( 'NONE',  ( 12.93548710985481698, 15.95582723538240266, 11.49999999999999645 ) ) ;
#31803=CARTESIAN_POINT ( 'NONE',  ( -120.5896316483122206, -24.52300882791530512, 0.6510814631126412566 ) ) ;
#31804=B_SPLINE_CURVE_WITH_KNOTS ( 'NONE', 3,
 ( #47095, #63839, #86643, #63332 ),
 .UNSPECIFIED., .F., .F.,
 ( 4, 4 ),
 ( 0.000000000000000000, 0.0001002978978728732653 ),
 .UNSPECIFIED. ) ;
#31805=CARTESIAN_POINT ( 'NONE',  ( -19.71520456405594857, 11.01310763156902972, 11.49999999999999645 ) ) ;
#31807=CARTESIAN_POINT ( 'NONE',  ( -99.52927036222322954, -25.31296297631381620, 4.031758516326467756 ) ) ;
#31808=CARTESIAN_POINT ( 'NONE',  ( -37.52287095715009713, -23.94994826722564696, -0.6494450866342743600 ) ) ;
#31810=LINE ( 'NONE', #352, #1337 ) ;
#31811=EDGE_CURVE ( 'NONE', #29757, #89989, #61424, .T. ) ;
#31812=FACE_OUTER_BOUND ( 'NONE', #33687, .T. ) ;
#31813=CARTESIAN_POINT ( 'NONE',  ( -75.62287095715005592, -23.47593901973091235, -1.443836447539004642 ) ) ;
#31816=ADVANCED_FACE ( 'NONE', ( #11446 ), #12439, .T. ) ;
#31818=CARTESIAN_POINT ( 'NONE',  ( 13.81544771398824345, -18.15223324129861382, 11.49999999999998934 ) ) ;
#31819=CARTESIAN_POINT ( 'NONE',  ( -74.50330917534071773, -24.34968618360933590, 0.1864209137778816416 ) ) ;
#31820=CARTESIAN_POINT ( 'NONE',  ( -96.54971732979119281, -24.34968618360933945, 0.1864209137778868874 ) ) ;
#31821=CARTESIAN_POINT ( 'NONE',  ( -104.5895376238167103, -24.66019654487199730, 8.947790411086122830 ) ) ;
#31822=CARTESIAN_POINT ( 'NONE',  ( 17.95543856985664277, -13.40637504462900331, 11.49999999999999645 ) ) ;
#31823=ORIENTED_EDGE ( 'NONE', *, *, #76331, .F. ) ;
#31824=CARTESIAN_POINT ( 'NONE',  ( -70.62287095715007013, -24.92604778743016780, 8.074972756849353672 ) ) ;
#31825=CARTESIAN_POINT ( 'NONE',  ( -4.809782828112996178, 21.40371668077904488, 11.49999999999998934 ) ) ;
#31826=CARTESIAN_POINT ( 'NONE',  ( -113.5228709571500758, -23.48783264082477373, -1.443836473390082586 ) ) ;
#31828=CARTESIAN_POINT ( 'NONE',  ( -34.58675657562977079, -24.35071581493542681, 9.817618358456032368 ) ) ;
#31831=CARTESIAN_POINT ( 'NONE',  ( -48.53097579249177329, -24.66019654487199730, 8.947790411086119278 ) ) ;
#31833=ORIENTED_EDGE ( 'NONE', *, *, #2318, .T. ) ;
#31834=AXIS2_PLACEMENT_3D ( 'NONE', #4017, #43576, #66437 ) ;
#31835=CARTESIAN_POINT ( 'NONE',  ( -18.53176153473302179, -8.692061069824589481, 11.49999999999998934 ) ) ;
#31836=ORIENTED_EDGE ( 'NONE', *, *, #6248, .F. ) ;
#31838=VERTEX_POINT ( 'NONE', #64772 ) ;
#31839=ORIENTED_EDGE ( 'NONE', *, *, #65845, .T. ) ;
#31840=CARTESIAN_POINT ( 'NONE',  ( -22.63574357292403860, -4.499050354539342322, -1.500000000000002220 ) ) ;
#31841=CARTESIAN_POINT ( 'NONE',  ( -102.5895376238167387, -24.66019654487199730, 8.947790411086126383 ) ) ;
#31842=CARTESIAN_POINT ( 'NONE',  ( -16.53579703214142427, -11.71821515807347680, -1.500000000000002220 ) ) ;
#31844=DIRECTION ( 'NONE',  ( -3.773278334453079618E-23, 0.9999999999976377785, 2.173523156925979975E-06 ) ) ;
#31845=CARTESIAN_POINT ( 'NONE',  ( -37.62287095715005592, -23.48783264082477373, -1.443836473390072372 ) ) ;
#31847=EDGE_CURVE ( 'NONE', #9262, #6118, #42024, .T. ) ;
#31848=CARTESIAN_POINT ( 'NONE',  ( -112.6228709571500559, -23.47593901973091235, -1.443836447538999312 ) ) ;
#31849=CARTESIAN_POINT ( 'NONE',  ( -63.52287095715006160, -24.64965694238575011, 8.947790433994201820 ) ) ;
#31850=CARTESIAN_POINT ( 'NONE',  ( -21.47443924280258187, -0.1944818460393343829, 11.49999999999999645 ) ) ;
#31851=EDGE_LOOP ( 'NONE', ( #668, #68850, #32828, #93073 ) ) ;
#31853=CARTESIAN_POINT ( 'NONE',  ( -61.55970306133350078, -23.73791477778911840, 11.05961554403170766 ) ) ;
#31854=VERTEX_POINT ( 'NONE', #3851 ) ;
#31855=CARTESIAN_POINT ( 'NONE',  ( -17.23291202157775359, 11.51834372740795231, -1.500000000000002220 ) ) ;
#31856=ADVANCED_FACE ( 'NONE', ( #18058 ), #57145, .F. ) ;
#31857=VERTEX_POINT ( 'NONE', #58140 ) ;
#31859=EDGE_LOOP ( 'NONE', ( #23836, #25906, #29946, #64706 ) ) ;
#31860=CARTESIAN_POINT ( 'NONE',  ( -111.5553594392847714, -23.96169478059714564, 10.65365249895717348 ) ) ;
#31861=DIRECTION ( 'NONE',  ( -3.773278334453079030E-23, 0.9999999999976377785, 2.173523156925979128E-06 ) ) ;
#31863=ORIENTED_EDGE ( 'NONE', *, *, #66367, .F. ) ;
#31864=CARTESIAN_POINT ( 'NONE',  ( -126.6228709571500559, -29.50250786944525672, 11.44777988621622633 ) ) ;
#31865=CARTESIAN_POINT ( 'NONE',  ( -42.59366545525777781, -24.15620529776628089, 10.23563542870661358 ) ) ;
#31866=CARTESIAN_POINT ( 'NONE',  ( -29.52342969602818812, -25.05915383044238354, 2.942153679875703531 ) ) ;
#31867=CARTESIAN_POINT ( 'NONE',  ( 21.95769793831392036, 2.030053023538682222, 11.49999999999999645 ) ) ;
#31868=CARTESIAN_POINT ( 'NONE',  ( -89.51816229286842486, -23.73791477778911840, 11.05961554403170410 ) ) ;
#31869=CARTESIAN_POINT ( 'NONE',  ( 0.2737972009257602091, 22.58959237946467624, 11.49999999999998934 ) ) ;
#31871=CARTESIAN_POINT ( 'NONE',  ( -5.787726610425443674, -20.20099407548119075, -1.500000000000002220 ) ) ;
#31873=CARTESIAN_POINT ( 'NONE',  ( -46.65381096568098229, -23.73791477778911840, 11.05961554403171299 ) ) ;
#31874=ORIENTED_EDGE ( 'NONE', *, *, #75100, .T. ) ;
#31875=ORIENTED_EDGE ( 'NONE', *, *, #42646, .F. ) ;
#31877=CARTESIAN_POINT ( 'NONE',  ( -112.6228709571500559, -23.47593901973091235, -1.443836447538999312 ) ) ;
#31878=ORIENTED_EDGE ( 'NONE', *, *, #23941, .T. ) ;
#31879=CARTESIAN_POINT ( 'NONE',  ( 15.93590435955092843, -13.91358336426615239, 11.49999999999998934 ) ) ;
#31880=CARTESIAN_POINT ( 'NONE',  ( -117.6228709571500559, -29.50248528299804818, 1.056150453629045360 ) ) ;
#31881=CARTESIAN_POINT ( 'NONE',  ( -62.62287095715004881, -24.64965695001468404, 8.947790433994185832 ) ) ;
#31882=DIRECTION ( 'NONE',  ( -1.000000000000000000, -3.773278334444167608E-23, -8.201307833595939069E-29 ) ) ;
#31883=DIRECTION ( 'NONE',  ( -3.773278334453079030E-23, 0.9999999999976377785, 2.173523156925979128E-06 ) ) ;
#31885=CARTESIAN_POINT ( 'NONE',  ( -0.9539927174334467130, 22.11892580961223587, -1.500000000000002220 ) ) ;
#31887=ORIENTED_EDGE ( 'NONE', *, *, #80354, .T. ) ;
#31889=CARTESIAN_POINT ( 'NONE',  ( -64.62287095715007013, -23.95044443724992078, 10.65354141964650125 ) ) ;
#31890=CARTESIAN_POINT ( 'NONE',  ( -40.29378138501845541, -25.30381737957640098, 5.537529357773589567 ) ) ;
#31892=DIRECTION ( 'NONE',  ( 3.773278334444167608E-23, -1.000000000000000000, 0.000000000000000000 ) ) ;
#31894=CARTESIAN_POINT ( 'NONE',  ( -19.46337940159461866, -0.4807646128305608779, 11.49999999999998934 ) ) ;
#31895=CARTESIAN_POINT ( 'NONE',  ( -3.722501342491481235, -21.08806747394077519, -1.500000000000002220 ) ) ;
#31897=CARTESIAN_POINT ( 'NONE',  ( -60.49711091220426340, -24.40133493613624083, 9.663955038888266458 ) ) ;
#31899=CARTESIAN_POINT ( 'NONE',  ( -37.52287095715006870, -23.47593901973090524, -1.443836447538997314 ) ) ;
#31900=CARTESIAN_POINT ( 'NONE',  ( 9.008567143757492346, 20.83016157428379955, -1.500000000000002220 ) ) ;
#31902=CARTESIAN_POINT ( 'NONE',  ( -103.6228709571500985, -24.34917612406838572, 0.1852690917426675354 ) ) ;
#31904=CARTESIAN_POINT ( 'NONE',  ( -14.63867168220055781, -13.42826565525684579, 11.49999999999999645 ) ) ;
#31908=CARTESIAN_POINT ( 'NONE',  ( -115.5895376238167245, -23.47596703998600631, 11.44779298504227683 ) ) ;
#31909=CARTESIAN_POINT ( 'NONE',  ( -98.52287095715006160, -23.47596703998600631, 11.44779298504228215 ) ) ;
#31910=ORIENTED_EDGE ( 'NONE', *, *, #53502, .F. ) ;
#31914=CARTESIAN_POINT ( 'NONE',  ( -75.55620429048340725, -24.99132157543166954, 2.256160258750667946 ) ) ;
#31915=CARTESIAN_POINT ( 'NONE',  ( -20.21959982808627032, -7.803091810188320210, -1.500000000000002220 ) ) ;
#31916=CARTESIAN_POINT ( 'NONE',  ( -56.49248187012878475, -24.51419770103157347, 9.386484678747180510 ) ) ;
#31917=CARTESIAN_POINT ( 'NONE',  ( 16.96702763494397104, -9.608290155750392358, -1.500000000000002220 ) ) ;
#31919=EDGE_CURVE ( 'NONE', #62364, #38339, #28813, .T. ) ;
#31920=CARTESIAN_POINT ( 'NONE',  ( -65.62287095715005592, -29.50247984919015209, -1.443849546365055359 ) ) ;
#31921=ORIENTED_EDGE ( 'NONE', *, *, #40680, .T. ) ;
#31923=CARTESIAN_POINT ( 'NONE',  ( 16.53694760393551988, -11.94906295602464397, 11.49999999999999645 ) ) ;
#31924=CARTESIAN_POINT ( 'NONE',  ( -80.58711764223190244, -24.63355581998386157, 0.9682620441943954326 ) ) ;
#31925=EDGE_CURVE ( 'NONE', #72799, #83369, #23838, .T. ) ;
#31927=ORIENTED_EDGE ( 'NONE', *, *, #52288, .F. ) ;
#31928=CARTESIAN_POINT ( 'NONE',  ( -0.09721816884246162194, -21.79143440635900220, 10.49653219292474482 ) ) ;
#31930=CARTESIAN_POINT ( 'NONE',  ( -48.99007696559036162, -25.25214574776337528, 5.618156514524055289 ) ) ;
#31931=CARTESIAN_POINT ( 'NONE',  ( -40.58148300679458487, -24.73531770709094957, 8.716586749053510275 ) ) ;
#31933=CARTESIAN_POINT ( 'NONE',  ( 17.77915467781788195, 9.360003092772107181, -1.500000000000002220 ) ) ;
#31935=ORIENTED_EDGE ( 'NONE', *, *, #11464, .F. ) ;
#31937=AXIS2_PLACEMENT_3D ( 'NONE', #59086, #4294, #65714 ) ;
#31938=CARTESIAN_POINT ( 'NONE',  ( -17.89994474767736676, -14.32179853049041363, 11.49999999999999645 ) ) ;
#31939=CARTESIAN_POINT ( 'NONE',  ( 6.262736145392394427, -21.83385498489561272, 11.49999999999998934 ) ) ;
#31940=ORIENTED_EDGE ( 'NONE', *, *, #3278, .T. ) ;
#31941=CARTESIAN_POINT ( 'NONE',  ( -45.52287095715007581, -24.15431212366390668, -0.2830839119429377493 ) ) ;
#31945=CARTESIAN_POINT ( 'NONE',  ( -30.57287095715005520, -25.00045060868233904, 2.199475715307360968 ) ) ;
#31946=CARTESIAN_POINT ( 'NONE',  ( -128.6237108470990336, -24.35071581493544102, 9.817618358456018157 ) ) ;
#31947=CARTESIAN_POINT ( 'NONE',  ( -58.56686834977553247, -23.48783264082477018, -1.443836473390093689 ) ) ;
#31949=CARTESIAN_POINT ( 'NONE',  ( 18.38310620586021571, 8.829655622120887060, -1.500000000000002220 ) ) ;
#31951=CARTESIAN_POINT ( 'NONE',  ( -5.582908757718670678, 22.30220962497079285, -1.500000000000002220 ) ) ;
#31952=LINE ( 'NONE', #2016, #47028 ) ;
#31954=ORIENTED_EDGE ( 'NONE', *, *, #22910, .F. ) ;
#31955=CARTESIAN_POINT ( 'NONE',  ( -114.5228709571500616, -24.51387760970725083, 9.387446482453398744 ) ) ;
#31958=CARTESIAN_POINT ( 'NONE',  ( 1.434216325579209750, -21.26356369375713484, 11.49999999999999645 ) ) ;
#31959=ORIENTED_EDGE ( 'NONE', *, *, #60526, .F. ) ;
#31961=CARTESIAN_POINT ( 'NONE',  ( -13.35739915041183323, 17.77566839534079435, -1.500000000000002220 ) ) ;
#31962=CARTESIAN_POINT ( 'NONE',  ( 18.09409571311175569, -9.955296453752364272, 11.49999999999998934 ) ) ;
#31963=ADVANCED_FACE ( 'NONE', ( #35790 ), #44405, .T. ) ;
#31964=VECTOR ( 'NONE', #22928, 1000.000000000000114 ) ;
#31965=ORIENTED_EDGE ( 'NONE', *, *, #64466, .T. ) ;
#31966=CARTESIAN_POINT ( 'NONE',  ( -108.9567485977555634, -25.31627131983182721, 4.232820541622530186 ) ) ;
#31967=EDGE_CURVE ( 'NONE', #10120, #11757, #75331, .T. ) ;
#31968=FACE_OUTER_BOUND ( 'NONE', #87595, .T. ) ;
#31973=DIRECTION ( 'NONE',  ( -3.773278334453079618E-23, 0.9999999999976377785, 2.173523156925979975E-06 ) ) ;
#31974=B_SPLINE_CURVE_WITH_KNOTS ( 'NONE', 3,
 ( #90, #39145, #45272, #53884, #16308, #60997 ),
 .UNSPECIFIED., .F., .F.,
 ( 4, 2, 4 ),
 ( 0.000000000000000000, 0.001380764517854764098, 0.002761529035709528197 ),
 .UNSPECIFIED. ) ;
#31976=CARTESIAN_POINT ( 'NONE',  ( -0.6367455441941621830, -20.85161220577290919, -1.500000000000002220 ) ) ;
#31977=CARTESIAN_POINT ( 'NONE',  ( 21.05697796394607835, 5.830696701215154043, 11.49999999999999645 ) ) ;
#31980=CARTESIAN_POINT ( 'NONE',  ( 18.89768980500364037, -12.13386209897132773, 11.49999999999998934 ) ) ;
#31981=CARTESIAN_POINT ( 'NONE',  ( -118.5210650335506699, -23.73791477778912551, 11.05961554403169878 ) ) ;
#31982=CARTESIAN_POINT ( 'NONE',  ( -58.52287095715006870, -23.96127896941631974, -0.6493128931038022467 ) ) ;
#31984=ORIENTED_EDGE ( 'NONE', *, *, #9163, .F. ) ;
#31986=ORIENTED_EDGE ( 'NONE', *, *, #50384, .T. ) ;
#31987=ORIENTED_EDGE ( 'NONE', *, *, #42038, .T. ) ;
#31988=CARTESIAN_POINT ( 'NONE',  ( -19.74196057798672399, -8.316236533413031040, -1.500000000000002220 ) ) ;
#31989=CARTESIAN_POINT ( 'NONE',  ( -18.60458529277170214, -12.42720982490441095, 11.49999999999999645 ) ) ;
#31990=ORIENTED_EDGE ( 'NONE', *, *, #76209, .T. ) ;
#31991=CARTESIAN_POINT ( 'NONE',  ( -20.97943885474387216, 2.004451313549292735, -1.500000000000002220 ) ) ;
#31993=CARTESIAN_POINT ( 'NONE',  ( 16.68016870136555596, 10.92824754362290385, -1.500000000000002220 ) ) ;
#31995=CARTESIAN_POINT ( 'NONE',  ( -43.52287095715006160, -23.48786465467240347, 11.44779295918255180 ) ) ;
#31996=CARTESIAN_POINT ( 'NONE',  ( 19.49364837986538745, 10.19379059548657551, -1.500000000000002220 ) ) ;
#31998=ORIENTED_EDGE ( 'NONE', *, *, #1446, .F. ) ;
#31999=PLANE ( 'NONE',  #45363 ) ;
#32000=CARTESIAN_POINT ( 'NONE',  ( -70.52287095715007581, -23.47593901973090524, -1.443836447538997092 ) ) ;
#32001=CARTESIAN_POINT ( 'NONE',  ( -11.21968731015968856, -17.59241007644406096, 11.49999999999999645 ) ) ;
#32002=AXIS2_PLACEMENT_3D ( 'NONE', #75772, #84394, #44848 ) ;
#32004=DIRECTION ( 'NONE',  ( -3.773278334453079618E-23, 0.9999999999976377785, 2.173523156925979975E-06 ) ) ;
#32006=CARTESIAN_POINT ( 'NONE',  ( -90.55620429048339304, -25.00158670708909625, 2.256160236439166855 ) ) ;
#32007=CARTESIAN_POINT ( 'NONE',  ( 5.124585555570928541, 20.71496159572455653, -1.500000000000002220 ) ) ;
#32009=CARTESIAN_POINT ( 'NONE',  ( -50.40445135320379677, -25.19502912051677868, 3.293943094755626078 ) ) ;
#32010=CARTESIAN_POINT ( 'NONE',  ( -96.52287095715001897, -24.66019654487199730, 8.947790411086115725 ) ) ;
#32011=CARTESIAN_POINT ( 'NONE',  ( -54.62287095715005592, -29.50248528299804818, 1.056150453629033370 ) ) ;
#32012=CARTESIAN_POINT ( 'NONE',  ( 3.584315319034878211, 22.25550262085195286, -1.500000000000002220 ) ) ;
#32013=DIRECTION ( 'NONE',  ( 0.000000000000000000, -0.9999999999976377785, -2.173523156925979975E-06 ) ) ;
#32016=CARTESIAN_POINT ( 'NONE',  ( -68.22287095715010707, -23.47593901973090524, -1.443836447538997980 ) ) ;
#32017=CARTESIAN_POINT ( 'NONE',  ( 3.778003860535555702, 19.31821889988591323, 11.49999999999999645 ) ) ;
#32018=PLANE ( 'NONE',  #24413 ) ;
#32019=DIRECTION ( 'NONE',  ( -1.000000000000000000, -3.773278334444166432E-23, -8.201307841325785021E-29 ) ) ;
#32021=CARTESIAN_POINT ( 'NONE',  ( -111.5228709571500616, -24.33832256527048088, 0.1851278514138661180 ) ) ;
#32023=CARTESIAN_POINT ( 'NONE',  ( -105.5228709571500758, -23.48786465467241769, 11.44779295918253936 ) ) ;
#32025=B_SPLINE_CURVE_WITH_KNOTS ( 'NONE', 3,
 ( #92596, #23074, #16468, #85994, #38814, #8370 ),
 .UNSPECIFIED., .F., .F.,
 ( 4, 2, 4 ),
 ( 0.000000000000000000, 0.001380901958385388545, 0.002761803916770777089 ),
 .UNSPECIFIED. ) ;
#32026=CARTESIAN_POINT ( 'NONE',  ( -77.62287095715009855, -23.47596703998600631, 11.44779298504227683 ) ) ;
#32027=CARTESIAN_POINT ( 'NONE',  ( 19.69962056004252560, 1.334664424591413434, -1.500000000000002220 ) ) ;
#32028=ORIENTED_EDGE ( 'NONE', *, *, #45111, .F. ) ;
#32034=VERTEX_POINT ( 'NONE', #51517 ) ;
#32036=CARTESIAN_POINT ( 'NONE',  ( -107.6228709571500985, -23.96127896941632685, -0.6493128931037773777 ) ) ;
#32037=CARTESIAN_POINT ( 'NONE',  ( -70.35895856474229504, -25.30161620421289470, 5.313173632321669615 ) ) ;
#32038=CARTESIAN_POINT ( 'NONE',  ( -99.52287095715006160, -29.50247984919015209, -1.443849546365050029 ) ) ;
#32039=CARTESIAN_POINT ( 'NONE',  ( -85.62287095715004170, -23.48783264082478794, -1.443836473390063713 ) ) ;
#32043=CARTESIAN_POINT ( 'NONE',  ( -6.099057486122481997, -19.05896565686126110, -1.500000000000002220 ) ) ;
#32045=CARTESIAN_POINT ( 'NONE',  ( -58.62287095715004170, -23.72747288104442021, -1.053458166803663110 ) ) ;
#32050=CARTESIAN_POINT ( 'NONE',  ( -35.60242693951278170, -24.15503026093914940, -0.2815557561904327155 ) ) ;
#32051=CARTESIAN_POINT ( 'NONE',  ( -108.5228709571500758, -23.47593901973090524, -1.443836447538996204 ) ) ;
#32052=CARTESIAN_POINT ( 'NONE',  ( -119.1722404401672577, -25.37154127157532102, 4.079011290487098762 ) ) ;
#32053=CARTESIAN_POINT ( 'NONE',  ( -83.55852065756700142, -23.73766607897670511, -1.055555164236456900 ) ) ;
#32055=CARTESIAN_POINT ( 'NONE',  ( -98.87653003804196317, -25.11539320716599732, 2.804431449967498491 ) ) ;
#32057=CARTESIAN_POINT ( 'NONE',  ( 0.7445296356392017145, -20.29553345556499622, 11.49999999999998934 ) ) ;
#32059=VECTOR ( 'NONE', #84532, 1000.000000000000114 ) ;
#32060=CARTESIAN_POINT ( 'NONE',  ( -59.59290457170049393, -24.15620529776628445, 10.23563542870661180 ) ) ;
#32064=CARTESIAN_POINT ( 'NONE',  ( -19.13055903301823335, -6.388282315271819556, -1.500000000000002220 ) ) ;
#32065=CARTESIAN_POINT ( 'NONE',  ( -0.2625952501129409367, 21.13516572482953748, 11.49999999999999645 ) ) ;
#32066=CARTESIAN_POINT ( 'NONE',  ( 0.7503028313155074569, 22.12739137992853955, 11.49999999999998934 ) ) ;
#32068=CARTESIAN_POINT ( 'NONE',  ( 7.805751503010069037, -19.01748540344778959, -1.500000000000002220 ) ) ;
#32070=ORIENTED_EDGE ( 'NONE', *, *, #34769, .T. ) ;
#32071=DIRECTION ( 'NONE',  ( -3.773278334453079618E-23, 0.9999999999976377785, 2.173523156925979975E-06 ) ) ;
#32072=ORIENTED_EDGE ( 'NONE', *, *, #31698, .T. ) ;
#32074=CARTESIAN_POINT ( 'NONE',  ( -109.5228709571500616, -23.47596703998600631, 11.44779298504228038 ) ) ;
#32076=ORIENTED_EDGE ( 'NONE', *, *, #97324, .F. ) ;
#32078=CARTESIAN_POINT ( 'NONE',  ( -111.0603964109058808, -25.15397636573018403, 3.025211319968325263 ) ) ;
#32080=CARTESIAN_POINT ( 'NONE',  ( -68.54453206456847170, -24.35071581493542681, 9.817618358456032368 ) ) ;
#32081=CARTESIAN_POINT ( 'NONE',  ( 16.32338804990218151, -12.73490195939593406, -1.500000000000002220 ) ) ;
#32082=CARTESIAN_POINT ( 'NONE',  ( 20.80172415560569021, 6.174449132348904357, 11.49999999999999645 ) ) ;
#32086=CARTESIAN_POINT ( 'NONE',  ( -13.97600220251353953, -17.46790257487896270, 11.49999999999998934 ) ) ;
#32088=CARTESIAN_POINT ( 'NONE',  ( -47.62839470087014604, -24.51419770103156637, 9.386484678747176957 ) ) ;
#32089=CARTESIAN_POINT ( 'NONE',  ( -101.5228709571500758, -23.47596703998600631, 11.44779298504228215 ) ) ;
#32091=CARTESIAN_POINT ( 'NONE',  ( -118.1689436852049226, -25.31364285773404887, 6.500980107507735362 ) ) ;
#32092=CARTESIAN_POINT ( 'NONE',  ( -35.66629286559531664, -23.85049219812685095, 10.88485053497527488 ) ) ;
#32095=AXIS2_PLACEMENT_3D ( 'NONE', #23172, #7457, #47541 ) ;
#32099=CARTESIAN_POINT ( 'NONE',  ( 21.14167878903947084, -0.5806874866175276706, -1.500000000000002220 ) ) ;
#32101=CARTESIAN_POINT ( 'NONE',  ( -50.53935553097652900, -24.52300882791529801, 0.6510814631126389251 ) ) ;
#32102=CARTESIAN_POINT ( 'NONE',  ( -18.25314811174894913, -11.95880190493418738, 11.49999999999998934 ) ) ;
#32103=CARTESIAN_POINT ( 'NONE',  ( -95.62287095715005592, -29.50249982740957577, 7.747779886224967605 ) ) ;
#32105=CARTESIAN_POINT ( 'NONE',  ( -107.5228709571500616, -24.50216790748204332, 0.6166512839542614977 ) ) ;
#32107=CARTESIAN_POINT ( 'NONE',  ( -21.66901994843296819, -2.608494568651300138, -1.500000000000002220 ) ) ;
#32108=CARTESIAN_POINT ( 'NONE',  ( -95.52287095715006160, -25.00158670708909980, 2.256160236439166411 ) ) ;
#32109=VERTEX_POINT ( 'NONE', #29163 ) ;
#32111=DIRECTION ( 'NONE',  ( -3.773278334453079030E-23, 0.9999999999976377785, 2.173523156925979128E-06 ) ) ;
#32112=EDGE_LOOP ( 'NONE', ( #92903, #8626, #63235, #33329 ) ) ;
#32114=CARTESIAN_POINT ( 'NONE',  ( -83.52287095715006160, -29.50248528299804818, 1.056150453629038477 ) ) ;
#32115=B_SPLINE_CURVE_WITH_KNOTS ( 'NONE', 3,
 ( #41851, #65201, #80894, #26612 ),
 .UNSPECIFIED., .F., .F.,
 ( 4, 4 ),
 ( 0.08055752415614364503, 0.08956395542825920653 ),
 .UNSPECIFIED. ) ;
#32116=VERTEX_POINT ( 'NONE', #76320 ) ;
#32118=ORIENTED_EDGE ( 'NONE', *, *, #76134, .T. ) ;
#32119=CARTESIAN_POINT ( 'NONE',  ( -27.68651082257923335, -24.77145582263907286, 2.274903367125437281 ) ) ;
#32120=CARTESIAN_POINT ( 'NONE',  ( -82.51746576141199796, -23.73766607897671577, -1.055555164236435362 ) ) ;
#32121=CARTESIAN_POINT ( 'NONE',  ( 6.411417644607832145, 20.24884965431308714, -1.500000000000002220 ) ) ;
#32122=CARTESIAN_POINT ( 'NONE',  ( -94.52217265877372654, -23.48783264082477018, -1.443836473390086805 ) ) ;
#32123=CARTESIAN_POINT ( 'NONE',  ( -30.60993385648455956, -24.45056191361606679, 9.787827635114012992 ) ) ;
#32124=PLANE ( 'NONE',  #58344 ) ;
#32126=CARTESIAN_POINT ( 'NONE',  ( -0.1161231997828221785, -19.40653004597026410, 11.49999999999998934 ) ) ;
#32127=FACE_OUTER_BOUND ( 'NONE', #23317, .T. ) ;
#32129=CARTESIAN_POINT ( 'NONE',  ( -17.32436372870746055, -8.985247798433253053, 11.49999999999999645 ) ) ;
#32130=CARTESIAN_POINT ( 'NONE',  ( -36.52287095715006870, -24.64898659630367916, 1.056161002820819261 ) ) ;
#32132=CARTESIAN_POINT ( 'NONE',  ( -107.6228709571500701, -24.65952944569304961, 1.056160979905703901 ) ) ;
#32133=VERTEX_POINT ( 'NONE', #22033 ) ;
#32134=CARTESIAN_POINT ( 'NONE',  ( -103.6228709571500559, -23.47593901973091235, -1.443836447539001089 ) ) ;
#32135=CARTESIAN_POINT ( 'NONE',  ( -113.6228709571500417, -23.47596703998600631, 11.44779298504227860 ) ) ;
#32137=CARTESIAN_POINT ( 'NONE',  ( -93.59740417728193052, -23.73791477778911840, 11.05961554403170410 ) ) ;
#32138=CARTESIAN_POINT ( 'NONE',  ( -16.89733858281218204, -10.06102416988892934, 11.49999999999998934 ) ) ;
#32139=B_SPLINE_SURFACE_WITH_KNOTS ( 'NONE', 3, 1, ( 
 ( #58847, #60358 ),
 ( #29883, #75047 ),
 ( #59339, #60852 ),
 ( #19762, #67458 ),
 ( #81682, #98383 ),
 ( #38992, #15154 ),
 ( #70453, #69449 ),
 ( #68948, #69944 ),
 ( #76538, #85672 ),
 ( #62863, #23762 ),
 ( #92276, #14654 ),
 ( #22753, #53737 ),
 ( #45618, #99872 ),
 ( #46120, #938 ),
 ( #61851, #30380 ),
 ( #8042, #9045 ),
 ( #37999, #77045 ),
 ( #47624, #22252 ),
 ( #93272, #39997 ) ),
 .UNSPECIFIED., .F., .F., .F.,
 ( 4, 1, 1, 1, 1, 1, 1, 1, 1, 1, 1, 1, 1, 1, 1, 1, 4 ),
 ( 2, 2 ),
 ( 0.000000000000000000, 0.05885358602866869876, 0.1163154589633517422, 0.1726748434114566133, 0.2287803868809005492, 0.2845803591252761278, 0.3402565063845458537, 0.3966298050124581476, 0.4535072628751937174, 0.5123181897799959916, 0.5726484440568331280, 0.6360219358218018870, 0.7023629463891940539, 0.7714830560569314599, 0.8441844774899029957, 0.9200697939721571572, 1.000000000000000000 ),
 ( 0.000000000000000000, 1.000000000000000000 ),
 .UNSPECIFIED. ) ;
#32140=ORIENTED_EDGE ( 'NONE', *, *, #77702, .F. ) ;
#32141=CARTESIAN_POINT ( 'NONE',  ( 21.52761780497506905, -1.784033869580059939, 11.49999999999998934 ) ) ;
#32143=CARTESIAN_POINT ( 'NONE',  ( -121.6228709571500417, -24.64898659630368627, 1.056161002820833028 ) ) ;
#32144=CARTESIAN_POINT ( 'NONE',  ( -22.67921066581790868, 4.291001918001082771, -1.500000000000002220 ) ) ;
#32145=EDGE_CURVE ( 'NONE', #38706, #46190, #59134, .T. ) ;
#32146=B_SPLINE_CURVE_WITH_KNOTS ( 'NONE', 3,
 ( #20599, #91605, #37340, #66807 ),
 .UNSPECIFIED., .F., .F.,
 ( 4, 4 ),
 ( 0.7203002732715262368, 0.7293067045436417706 ),
 .UNSPECIFIED. ) ;
#32149=DIRECTION ( 'NONE',  ( -3.773278334453079030E-23, 0.9999999999976377785, 2.173523156925979128E-06 ) ) ;
#32150=CARTESIAN_POINT ( 'NONE',  ( -121.5181176591963066, -24.66019654487200441, 8.947790411086119278 ) ) ;
#32151=CARTESIAN_POINT ( 'NONE',  ( -64.62287095715005592, -24.51387760970723662, 9.387446482453425389 ) ) ;
#32152=CARTESIAN_POINT ( 'NONE',  ( -111.1265005993262491, -25.29823862383007338, 3.068069378922468893 ) ) ;
#32153=CARTESIAN_POINT ( 'NONE',  ( -124.5895376238167387, -23.48786465467241769, 11.44779295918253759 ) ) ;
#32154=B_SPLINE_CURVE_WITH_KNOTS ( 'NONE', 3,
 ( #21281, #46016, #93163, #46507 ),
 .UNSPECIFIED., .F., .F.,
 ( 4, 4 ),
 ( 0.000000000000000000, 9.999999999998897304E-05 ),
 .UNSPECIFIED. ) ;
#32155=CARTESIAN_POINT ( 'NONE',  ( -49.55620429048340014, -23.47593901973091235, -1.443836447539009749 ) ) ;
#32156=CARTESIAN_POINT ( 'NONE',  ( -6.132916590032589710, 18.96384228413732842, 11.49999999999998934 ) ) ;
#32158=CARTESIAN_POINT ( 'NONE',  ( -75.57899585548300081, -25.00182538069147142, 7.747789668545045139 ) ) ;
#32159=CARTESIAN_POINT ( 'NONE',  ( -15.51018552496569392, -12.33189742059753868, -1.500000000000002220 ) ) ;
#32163=CARTESIAN_POINT ( 'NONE',  ( -39.89740106121153929, -25.29116539929970386, 2.930847754509050329 ) ) ;
#32164=PLANE ( 'NONE',  #89658 ) ;
#32165=CARTESIAN_POINT ( 'NONE',  ( -9.423985339279758122, -18.44656043379632848, 11.49999999999999645 ) ) ;
#32167=CARTESIAN_POINT ( 'NONE',  ( -40.62287095715004170, -24.99132157543083466, 2.256160258750667502 ) ) ;
#32168=B_SPLINE_CURVE_WITH_KNOTS ( 'NONE', 3,
 ( #73066, #73556, #81666, #58342, #65967, #53221 ),
 .UNSPECIFIED., .F., .F.,
 ( 4, 2, 4 ),
 ( 6.391158118958419274E-06, 0.001387004593080783327, 0.002767618028042608501 ),
 .UNSPECIFIED. ) ;
#32169=CARTESIAN_POINT ( 'NONE',  ( -15.20078144808659992, 16.97451310947862169, 11.49999999999999645 ) ) ;
#32171=FACE_OUTER_BOUND ( 'NONE', #69309, .T. ) ;
#32172=CARTESIAN_POINT ( 'NONE',  ( -69.47493225014638085, -25.19029820154286980, 6.676482576448054651 ) ) ;
#32173=ORIENTED_EDGE ( 'NONE', *, *, #73825, .F. ) ;
#32175=CARTESIAN_POINT ( 'NONE',  ( -0.5548696950099620828, -20.20177982057877841, -1.500000000000002220 ) ) ;
#32177=CARTESIAN_POINT ( 'NONE',  ( -49.52287095715006160, -24.65952944569304606, 1.056160979905693686 ) ) ;
#32180=CARTESIAN_POINT ( 'NONE',  ( -17.45619364963476627, 14.87644265977633573, -1.500000000000002220 ) ) ;
#32181=CARTESIAN_POINT ( 'NONE',  ( -41.72781200478040375, -25.23288469818084678, 3.583692438795834434 ) ) ;
#32182=CARTESIAN_POINT ( 'NONE',  ( -3.121018476474317183, -19.76494895549465980, -1.500000000000002220 ) ) ;
#32184=CARTESIAN_POINT ( 'NONE',  ( -36.62287095715005592, -24.64965695001467694, 8.947790433994187609 ) ) ;
#32185=CARTESIAN_POINT ( 'NONE',  ( -20.97355972163249049, 0.1317905507124840780, 11.49999999999999645 ) ) ;
#32186=CARTESIAN_POINT ( 'NONE',  ( -86.62287095715001328, -24.50321055353805377, 9.387540953477522265 ) ) ;
#32187=CARTESIAN_POINT ( 'NONE',  ( -124.5915507283297217, -23.48783264082478084, -1.443836473390086361 ) ) ;
#32188=CARTESIAN_POINT ( 'NONE',  ( -21.92701646642465008, -2.088449908657787457, 11.49999999999998934 ) ) ;
#32190=ADVANCED_FACE ( 'NONE', ( #7313 ), #82942, .F. ) ;
#32191=EDGE_LOOP ( 'NONE', ( #12605, #49867, #38094, #83238 ) ) ;
#32193=FACE_OUTER_BOUND ( 'NONE', #69599, .T. ) ;
#32196=ORIENTED_EDGE ( 'NONE', *, *, #54068, .F. ) ;
#32197=ORIENTED_EDGE ( 'NONE', *, *, #69521, .F. ) ;
#32201=CARTESIAN_POINT ( 'NONE',  ( 17.38039551199336685, -10.77953091123627694, -1.500000000000002220 ) ) ;
#32202=B_SPLINE_CURVE_WITH_KNOTS ( 'NONE', 3,
 ( #94337, #17215, #92447, #32951 ),
 .UNSPECIFIED., .F., .F.,
 ( 4, 4 ),
 ( 0.000000000000000000, 0.0001000000000000028644 ),
 .UNSPECIFIED. ) ;
#32204=CARTESIAN_POINT ( 'NONE',  ( -79.52287095715010423, -23.72747288104470087, -1.053458166803226792 ) ) ;
#32207=CARTESIAN_POINT ( 'NONE',  ( -8.840690135214121170, 20.45858245768130956, 11.49999999999998934 ) ) ;
#32208=B_SPLINE_CURVE_WITH_KNOTS ( 'NONE', 3,
 ( #5064, #59357, #66000, #88314 ),
 .UNSPECIFIED., .F., .F.,
 ( 4, 4 ),
 ( 0.3900644599606266083, 0.3990708912327424196 ),
 .UNSPECIFIED. ) ;
#32209=CARTESIAN_POINT ( 'NONE',  ( -70.38567012983610027, -25.13346044137653124, 7.099803150338960478 ) ) ;
#32210=CARTESIAN_POINT ( 'NONE',  ( -88.62287095715004170, -23.48786465467241769, 11.44779295918254114 ) ) ;
#32212=CARTESIAN_POINT ( 'NONE',  ( -103.6228709571500559, -29.50247984919015209, -1.443849546365050029 ) ) ;
#32213=CARTESIAN_POINT ( 'NONE',  ( -118.5228709571500758, -24.64898659630368627, 1.056161002820833028 ) ) ;
#32214=CARTESIAN_POINT ( 'NONE',  ( -19.76906661924035191, -6.534152953431121347, 11.49999999999998934 ) ) ;
#32218=EDGE_CURVE ( 'NONE', #77901, #81257, #78286, .T. ) ;
#32220=CARTESIAN_POINT ( 'NONE',  ( -50.99155954085787812, -25.12217837880228188, 6.987757997958206069 ) ) ;
#32221=CARTESIAN_POINT ( 'NONE',  ( -19.40065202112720755, 8.109199488025859992, -1.500000000000002220 ) ) ;
#32222=EDGE_LOOP ( 'NONE', ( #62296, #51441, #25266, #53614 ) ) ;
#32223=FACE_OUTER_BOUND ( 'NONE', #50196, .T. ) ;
#32224=AXIS2_PLACEMENT_3D ( 'NONE', #60904, #43180, #60411 ) ;
#32227=ADVANCED_FACE ( 'NONE', ( #67748 ), #45897, .T. ) ;
#32229=CARTESIAN_POINT ( 'NONE',  ( -86.51068774892489444, -24.15620529776628445, 10.23563542870660292 ) ) ;
#32230=CARTESIAN_POINT ( 'NONE',  ( -60.62287095715002039, -24.82576562982391621, 8.398263435472967942 ) ) ;
#32231=CARTESIAN_POINT ( 'NONE',  ( -65.62287095715007013, -24.52323809116985132, 9.355190652339423707 ) ) ;
#32232=CARTESIAN_POINT ( 'NONE',  ( 22.14152233036116257, 1.636640089565777334, 11.49999999999999645 ) ) ;
#32233=ORIENTED_EDGE ( 'NONE', *, *, #53751, .F. ) ;
#32235=CARTESIAN_POINT ( 'NONE',  ( -54.52287095715006870, -24.64898659630367916, 1.056161002820821038 ) ) ;
#32236=VERTEX_POINT ( 'NONE', #24540 ) ;
#32237=CARTESIAN_POINT ( 'NONE',  ( -12.01393383709116947, -19.22582291892495121, 11.49999999999998934 ) ) ;
#32238=EDGE_CURVE ( 'NONE', #5385, #19525, #83147, .T. ) ;
#32244=ADVANCED_FACE ( 'NONE', ( #70725 ), #31653, .F. ) ;
#32247=CARTESIAN_POINT ( 'NONE',  ( 20.05498121024909253, 1.910150955369836812, -1.500000000000002220 ) ) ;
#32249=ORIENTED_EDGE ( 'NONE', *, *, #58304, .F. ) ;
#32250=AXIS2_PLACEMENT_3D ( 'NONE', #76221, #27332, #3011 ) ;
#32252=B_SPLINE_CURVE_WITH_KNOTS ( 'NONE', 3,
 ( #55065, #63183, #87508, #17993 ),
 .UNSPECIFIED., .F., .F.,
 ( 4, 4 ),
 ( 0.000000000000000000, 9.999999999998897304E-05 ),
 .UNSPECIFIED. ) ;
#32253=CARTESIAN_POINT ( 'NONE',  ( -20.38924965233672282, -9.335317855073830273, -1.500000000000002220 ) ) ;
#32254=ADVANCED_FACE ( 'NONE', ( #23525 ), #50749, .T. ) ;
#32256=VERTEX_POINT ( 'NONE', #31155 ) ;
#32257=CARTESIAN_POINT ( 'NONE',  ( -112.5504983259648384, -24.66019654487200086, 8.947790411086112172 ) ) ;
#32258=CARTESIAN_POINT ( 'NONE',  ( -94.59133804672956103, -24.15620529776628089, 10.23563542870660470 ) ) ;
#32259=CARTESIAN_POINT ( 'NONE',  ( -70.62287095715005592, -29.50248528299804818, 1.056150453629036701 ) ) ;
#32261=CARTESIAN_POINT ( 'NONE',  ( -71.70841769935766763, -25.24715640642683923, 6.192981443001071895 ) ) ;
#32262=CARTESIAN_POINT ( 'NONE',  ( -19.30006219055749739, -3.230038287793697283, 11.49999999999998934 ) ) ;
#32264=ORIENTED_EDGE ( 'NONE', *, *, #47520, .F. ) ;
#32265=CARTESIAN_POINT ( 'NONE',  ( 16.66814584454133907, -13.58961022886752978, 11.49999999999998934 ) ) ;
#32268=CARTESIAN_POINT ( 'NONE',  ( -113.5228709571500758, -24.51387760970726504, 9.387446482453402297 ) ) ;
#32269=CARTESIAN_POINT ( 'NONE',  ( -70.62287095715005592, -25.00182538069145011, 7.747789668545097541 ) ) ;
#32270=CARTESIAN_POINT ( 'NONE',  ( 20.38051395842347802, -10.57019977742728578, -1.500000000000002220 ) ) ;
#32272=VECTOR ( 'NONE', #33785, 1000.000000000000114 ) ;
#32273=EDGE_CURVE ( 'NONE', #73900, #21630, #37141, .T. ) ;
#32275=FACE_OUTER_BOUND ( 'NONE', #2394, .T. ) ;
#32276=CARTESIAN_POINT ( 'NONE',  ( -92.62287095715005592, -24.64898659630368627, 1.056161002820827921 ) ) ;
#32277=CARTESIAN_POINT ( 'NONE',  ( -13.93161493328335432, -14.37010051631055418, 11.49999999999999645 ) ) ;
#32281=LINE ( 'NONE', #331, #1876 ) ;
#32283=CARTESIAN_POINT ( 'NONE',  ( -50.62287095715005592, -23.85229601348995487, 10.88205029486209341 ) ) ;
#32284=EDGE_CURVE ( 'NONE', #26504, #84981, #15507, .T. ) ;
#32285=CARTESIAN_POINT ( 'NONE',  ( 5.219777686717518961, -21.12652377152128480, 11.49999999999998934 ) ) ;
#32287=CARTESIAN_POINT ( 'NONE',  ( 0.7877182283408599162, 19.66719298131377514, -1.500000000000002220 ) ) ;
#32289=EDGE_CURVE ( 'NONE', #21092, #45475, #19108, .T. ) ;
#32291=CARTESIAN_POINT ( 'NONE',  ( -109.7735670026218173, -25.31698141328030260, 5.109898621226075299 ) ) ;
#32293=CARTESIAN_POINT ( 'NONE',  ( -91.50434982067550038, -24.66019654487199730, 8.947790411086115725 ) ) ;
#32295=CARTESIAN_POINT ( 'NONE',  ( -17.31529204923715071, 11.11782870402162260, 11.49999999999999645 ) ) ;
#32297=CARTESIAN_POINT ( 'NONE',  ( -120.5177549675304647, -24.63355581998386157, 0.9682620441943888823 ) ) ;
#32298=CARTESIAN_POINT ( 'NONE',  ( -8.787219534579676861, -20.84281209399103929, 11.49999999999999645 ) ) ;
#32300=CARTESIAN_POINT ( 'NONE',  ( -46.62287095715004170, -23.73907113216991860, -1.053371485793232587 ) ) ;
#32302=CARTESIAN_POINT ( 'NONE',  ( -125.5903894658442255, -24.15602025860897584, 10.28564288303534013 ) ) ;
#32305=CARTESIAN_POINT ( 'NONE',  ( -25.59878527050454622, -24.61459625492054215, 6.005086935496544598 ) ) ;
#32306=CARTESIAN_POINT ( 'NONE',  ( -41.62287095715006302, -24.66019654487199020, 8.947790411086135265 ) ) ;
#32309=CARTESIAN_POINT ( 'NONE',  ( -79.36292229018619082, -25.31596392387344352, 5.750285860338011368 ) ) ;
#32310=CARTESIAN_POINT ( 'NONE',  ( 16.54545882101025711, 15.75737887292823558, -1.500000000000002220 ) ) ;
#32311=CARTESIAN_POINT ( 'NONE',  ( -104.5228709571500758, -24.50216790748206108, 0.6166512839542541702 ) ) ;
#32312=AXIS2_PLACEMENT_3D ( 'NONE', #55413, #8229, #93448 ) ;
#32313=CARTESIAN_POINT ( 'NONE',  ( -115.5228709571500758, -24.14406661686763655, 10.28769366194076795 ) ) ;
#32314=CARTESIAN_POINT ( 'NONE',  ( -63.61015071180399616, -23.48786465467241413, 11.44779295918254824 ) ) ;
#32315=CARTESIAN_POINT ( 'NONE',  ( 18.89768980500364037, -12.13386209897132773, 11.49999999999999645 ) ) ;
#32316=ORIENTED_EDGE ( 'NONE', *, *, #21124, .F. ) ;
#32318=DIRECTION ( 'NONE',  ( -3.773278334453079618E-23, 0.9999999999976377785, 2.173523156925979975E-06 ) ) ;
#32319=CARTESIAN_POINT ( 'NONE',  ( -19.17877449816284496, 10.63638241594707345, -1.500000000000002220 ) ) ;
#32322=CARTESIAN_POINT ( 'NONE',  ( -44.64054216518013618, -24.15620529776627734, 10.23563542870660470 ) ) ;
#32324=ORIENTED_EDGE ( 'NONE', *, *, #6230, .F. ) ;
#32325=CARTESIAN_POINT ( 'NONE',  ( -112.6228709571500701, -23.48786465467241769, 11.44779295918254114 ) ) ;
#32328=CARTESIAN_POINT ( 'NONE',  ( -0.3173379506236611580, 20.48240526196808631, 11.49999999999998934 ) ) ;
#32330=ORIENTED_EDGE ( 'NONE', *, *, #22731, .T. ) ;
#32332=ORIENTED_EDGE ( 'NONE', *, *, #79863, .F. ) ;
#32333=CARTESIAN_POINT ( 'NONE',  ( -14.58522200957802184, -17.87834940746265389, 11.49999999999998934 ) ) ;
#32335=CARTESIAN_POINT ( 'NONE',  ( -20.07547297788957152, 3.163885811906596679, -1.500000000000002220 ) ) ;
#32336=ORIENTED_EDGE ( 'NONE', *, *, #12411, .T. ) ;
#32337=CARTESIAN_POINT ( 'NONE',  ( -50.62287095715005592, -29.50250243563736774, 8.947779886222146928 ) ) ;
#32338=CARTESIAN_POINT ( 'NONE',  ( -72.52287095715007581, -23.47593901973090169, -1.443836447538996870 ) ) ;
#32339=CARTESIAN_POINT ( 'NONE',  ( -101.5115004759412187, -25.24062753727274355, 6.352195226156559293 ) ) ;
#32341=CARTESIAN_POINT ( 'NONE',  ( -15.31780299886000485, -15.04297462106122474, 11.49999999999999645 ) ) ;
#32343=CARTESIAN_POINT ( 'NONE',  ( -75.60360656315280892, -23.85016227208580730, -0.8807180028928284221 ) ) ;
#32344=CARTESIAN_POINT ( 'NONE',  ( -104.6228709571500985, -24.33832256526968862, 0.1851278514119912566 ) ) ;
#32345=VERTEX_POINT ( 'NONE', #49907 ) ;
#32346=CARTESIAN_POINT ( 'NONE',  ( 18.38559056850662543, 9.607341378227904016, -1.500000000000002220 ) ) ;
#32347=ORIENTED_EDGE ( 'NONE', *, *, #50736, .F. ) ;
#32348=LINE ( 'NONE', #70926, #94461 ) ;
#32349=EDGE_LOOP ( 'NONE', ( #1882, #96805, #35131, #34727 ) ) ;
#32351=CARTESIAN_POINT ( 'NONE',  ( -111.5588673000302293, -23.48786465467241769, 11.44779295918254114 ) ) ;
#32352=CARTESIAN_POINT ( 'NONE',  ( -57.52287095715005449, -29.50250243563736774, 8.947779886222145151 ) ) ;
#32357=CARTESIAN_POINT ( 'NONE',  ( -125.6228709571500559, -24.99132157543083821, 2.256160258750667502 ) ) ;
#32358=CARTESIAN_POINT ( 'NONE',  ( -29.26457644120217338, -24.94536068527088091, 2.458381786851871365 ) ) ;
#32359=CARTESIAN_POINT ( 'NONE',  ( -19.13726171168348245, 10.91495894028074432, 11.49999999999999645 ) ) ;
#32360=EDGE_CURVE ( 'NONE', #19500, #95501, #5808, .T. ) ;
#32361=CARTESIAN_POINT ( 'NONE',  ( -89.64225548740091654, -23.48786465467241058, 11.44779295918254114 ) ) ;
#32362=CARTESIAN_POINT ( 'NONE',  ( -13.16310354753345990, -18.33534949228788236, -1.500000000000002220 ) ) ;
#32364=CARTESIAN_POINT ( 'NONE',  ( 17.94697546605861760, -10.91086909363634838, -1.500000000000002220 ) ) ;
#32365=ADVANCED_FACE ( 'NONE', ( #95062 ), #87447, .T. ) ;
#32367=ORIENTED_EDGE ( 'NONE', *, *, #72374, .F. ) ;
#32368=ORIENTED_EDGE ( 'NONE', *, *, #89197, .F. ) ;
#32373=ORIENTED_EDGE ( 'NONE', *, *, #7207, .F. ) ;
#32374=CARTESIAN_POINT ( 'NONE',  ( 18.68757921870947669, -9.911485057863893999, 11.49999999999998934 ) ) ;
#32376=CARTESIAN_POINT ( 'NONE',  ( -51.92774333234893192, -25.26040843124357238, 6.302625152703366318 ) ) ;
#32378=CARTESIAN_POINT ( 'NONE',  ( -121.5908097599731548, -23.96119346886880663, -0.6495511937832033622 ) ) ;
#32381=CARTESIAN_POINT ( 'NONE',  ( 19.22371909900314435, 11.20011194808016342, -1.500000000000002220 ) ) ;
#32382=CARTESIAN_POINT ( 'NONE',  ( -49.72218425784361528, -25.13941470960068969, 7.443037641556777828 ) ) ;
#32386=CARTESIAN_POINT ( 'NONE',  ( -37.54586441416935827, -24.15543982623907127, -0.2315651400026566831 ) ) ;
#32387=CARTESIAN_POINT ( 'NONE',  ( -43.62287095715004881, -23.73907113216990439, -1.053371485793232587 ) ) ;
#32388=AXIS2_PLACEMENT_3D ( 'NONE', #98866, #69807, #93128 ) ;
#32389=CARTESIAN_POINT ( 'NONE',  ( -100.5064038502849115, -24.83618233451451118, 1.606449574219533050 ) ) ;
#32391=EDGE_CURVE ( 'NONE', #81403, #20070, #48900, .T. ) ;
#32393=CARTESIAN_POINT ( 'NONE',  ( 8.918240691521024388, 17.32521578647535776, -1.500000000000002220 ) ) ;
#32395=CARTESIAN_POINT ( 'NONE',  ( -3.722501342491481235, -21.08806747394077519, 11.49999999999998934 ) ) ;
#32397=CARTESIAN_POINT ( 'NONE',  ( -60.48527586300784264, -24.83644354574317603, 8.397322867105112110 ) ) ;
#32398=CARTESIAN_POINT ( 'NONE',  ( -100.6228709571500701, -23.85229601348997264, 10.88205029486208275 ) ) ;
#32399=CARTESIAN_POINT ( 'NONE',  ( -100.8624150394625616, -25.27359993006566441, 3.378658782965809682 ) ) ;
#32400=CARTESIAN_POINT ( 'NONE',  ( 0.6941480231959694658, 22.73124288027050710, -1.500000000000002220 ) ) ;
#32402=B_SPLINE_CURVE_WITH_KNOTS ( 'NONE', 3,
 ( #13488, #20603, #75384, #67806, #91116, #21591 ),
 .UNSPECIFIED., .F., .F.,
 ( 4, 2, 4 ),
 ( 6.391158118969315506E-06, 0.001387004593080787881, 0.002767618028042606766 ),
 .UNSPECIFIED. ) ;
#32404=CARTESIAN_POINT ( 'NONE',  ( -98.63811850894654754, -23.48783264082476308, -1.443836473390089914 ) ) ;
#32406=CARTESIAN_POINT ( 'NONE',  ( -16.82575997001036328, 10.57904039763333159, 11.49999999999999645 ) ) ;
#32407=CARTESIAN_POINT ( 'NONE',  ( -123.5222519426676371, -23.48786465467241413, 11.44779295918253759 ) ) ;
#32413=CARTESIAN_POINT ( 'NONE',  ( -80.62287095715005592, -29.50250243563736774, 8.947779886222141599 ) ) ;
#32414=CARTESIAN_POINT ( 'NONE',  ( -5.395268184683536639, 21.00466093859614958, -1.500000000000002220 ) ) ;
#32415=DIRECTION ( 'NONE',  ( -1.000000000000000000, -3.773278334444166432E-23, -8.201307841325785021E-29 ) ) ;
#32416=CARTESIAN_POINT ( 'NONE',  ( -15.63568348323273227, -11.59263941501104966, -1.500000000000002220 ) ) ;
#32417=CARTESIAN_POINT ( 'NONE',  ( -55.63763619402278948, -24.52399227489126687, 9.353111116836526406 ) ) ;
#32418=ADVANCED_FACE ( 'NONE', ( #41278 ), #74238, .T. ) ;
#32419=ORIENTED_EDGE ( 'NONE', *, *, #83815, .T. ) ;
#32420=CARTESIAN_POINT ( 'NONE',  ( 18.16468007720714795, -9.286844270591712913, 11.49999999999999645 ) ) ;
#32421=CARTESIAN_POINT ( 'NONE',  ( -87.62287095715004170, -29.50250243563736774, 8.947779886222139822 ) ) ;
#32424=ORIENTED_EDGE ( 'NONE', *, *, #26170, .F. ) ;
#32425=CARTESIAN_POINT ( 'NONE',  ( -78.98769050135813075, -25.22659656181679821, 6.389866568871956254 ) ) ;
#32426=CARTESIAN_POINT ( 'NONE',  ( -95.52287095715007581, -23.84081130425358097, 10.88220057483157888 ) ) ;
#32428=CARTESIAN_POINT ( 'NONE',  ( -49.29568538784691611, -25.25138839280181102, 5.964271804705676416 ) ) ;
#32430=CARTESIAN_POINT ( 'NONE',  ( 15.80722972286721983, -12.41807379269815215, 11.49999999999998934 ) ) ;
#32431=CARTESIAN_POINT ( 'NONE',  ( -89.55620429048339304, -24.66019654487199375, 8.947790411086124607 ) ) ;
#32432=EDGE_LOOP ( 'NONE', ( #91859, #90705, #10657, #40136 ) ) ;
#32433=CARTESIAN_POINT ( 'NONE',  ( -66.56566600343955997, -23.48786465467241058, 11.44779295918254824 ) ) ;
#32434=CARTESIAN_POINT ( 'NONE',  ( -11.38079350637645959, -19.95400817559217899, 11.49999999999999645 ) ) ;
#32435=CARTESIAN_POINT ( 'NONE',  ( 10.71911242904675987, 20.06137936439360203, 11.49999999999998934 ) ) ;
#32438=CARTESIAN_POINT ( 'NONE',  ( -75.62287095715004170, -25.00182538069145366, 7.747789668545099317 ) ) ;
#32442=CARTESIAN_POINT ( 'NONE',  ( -70.62287095715004170, -23.48786465467241058, 11.44779295918254469 ) ) ;
#32444=CARTESIAN_POINT ( 'NONE',  ( -54.52287095715006870, -24.50216790748204332, 0.6166512839542456215 ) ) ;
#32445=CARTESIAN_POINT ( 'NONE',  ( -99.04404089887771079, -25.31200610177687338, 5.494369131775782122 ) ) ;
#32446=ORIENTED_EDGE ( 'NONE', *, *, #88733, .F. ) ;
#32448=CARTESIAN_POINT ( 'NONE',  ( 16.53694760393551988, -11.94906295602464397, -1.500000000000002220 ) ) ;
#32449=B_SPLINE_CURVE_WITH_KNOTS ( 'NONE', 3,
 ( #47449, #32209, #24594, #93601, #8882, #2784, #70287, #8378, #94614, #48954, #2285, #23587, #24096, #79384 ),
 .UNSPECIFIED., .F., .F.,
 ( 4, 2, 2, 2, 2, 2, 4 ),
 ( 0.000000000000000000, 0.0001838514736245833582, 0.0003677029472491667164, 0.0007354058944983334328, 0.001103108841747500041, 0.001286960315372091476, 0.001470811788996682912 ),
 .UNSPECIFIED. ) ;
#32450=ORIENTED_EDGE ( 'NONE', *, *, #6602, .T. ) ;
#32451=CARTESIAN_POINT ( 'NONE',  ( -21.48638390452810043, -8.140844714011898020, -1.500000000000002220 ) ) ;
#32454=CARTESIAN_POINT ( 'NONE',  ( -102.5228709571501042, -24.66019654487200441, 8.947790411086119278 ) ) ;
#32456=VECTOR ( 'NONE', #69938, 1000.000000000000114 ) ;
#32457=CARTESIAN_POINT ( 'NONE',  ( -116.4728709572981558, -25.30561156865042349, 5.197853587462041070 ) ) ;
#32458=CARTESIAN_POINT ( 'NONE',  ( -11.06822068739258391, -18.21809710261049275, 11.49999999999999645 ) ) ;
#32460=AXIS2_PLACEMENT_3D ( 'NONE', #67412, #75493, #67916 ) ;
#32461=VERTEX_POINT ( 'NONE', #90937 ) ;
#32462=CARTESIAN_POINT ( 'NONE',  ( -10.71655374829924767, -19.46388382022006525, 11.49999999999998934 ) ) ;
#32463=CARTESIAN_POINT ( 'NONE',  ( 19.46067915675286386, 6.892634557253153105, 11.49999999999998934 ) ) ;
#32466=FACE_OUTER_BOUND ( 'NONE', #61200, .T. ) ;
#32468=ADVANCED_FACE ( 'NONE', ( #82819 ), #21409, .F. ) ;
#32470=VERTEX_POINT ( 'NONE', #75701 ) ;
#32471=CARTESIAN_POINT ( 'NONE',  ( -49.52287095715006160, -23.48783264082477018, -1.443836473390095465 ) ) ;
#32472=ADVANCED_FACE ( 'NONE', ( #37651 ), #67620, .T. ) ;
#32474=CARTESIAN_POINT ( 'NONE',  ( 14.99592430652175956, 14.54719766626331889, -1.500000000000002220 ) ) ;
#32475=CARTESIAN_POINT ( 'NONE',  ( -17.41291239988371231, 13.16847401419012975, 11.49999999999999645 ) ) ;
#32477=CARTESIAN_POINT ( 'NONE',  ( -27.27372260060660736, -24.77993783887843904, 7.541612773693165295 ) ) ;
#32478=DIRECTION ( 'NONE',  ( 0.000000000000000000, -2.173523156925979552E-06, 0.9999999999976378895 ) ) ;
#32479=CARTESIAN_POINT ( 'NONE',  ( 17.90692129536829924, 13.62026984716248101, 11.49999999999998934 ) ) ;
#32480=EDGE_CURVE ( 'NONE', #98958, #62104, #56582, .T. ) ;
#32481=CARTESIAN_POINT ( 'NONE',  ( -118.5537731958665830, -24.35071581493543746, 9.817618358456021710 ) ) ;
#32484=ORIENTED_EDGE ( 'NONE', *, *, #79118, .T. ) ;
#32485=B_SPLINE_CURVE_WITH_KNOTS ( 'NONE', 3,
 ( #4488, #57292, #97325, #88226 ),
 .UNSPECIFIED., .F., .F.,
 ( 4, 4 ),
 ( 0.3690289907973323125, 0.3700297378380976165 ),
 .UNSPECIFIED. ) ;
#32488=B_SPLINE_CURVE_WITH_KNOTS ( 'NONE', 3,
 ( #84300, #47142, #64390, #94799 ),
 .UNSPECIFIED., .F., .F.,
 ( 4, 4 ),
 ( 0.1999286886604119962, 0.2089351199325275577 ),
 .UNSPECIFIED. ) ;
#32489=CARTESIAN_POINT ( 'NONE',  ( -99.41830603981939873, -25.26221207296531546, 6.591151539727326814 ) ) ;
#32491=CARTESIAN_POINT ( 'NONE',  ( -3.722501342491481235, -21.08806747394077519, -1.500000000000002220 ) ) ;
#32492=EDGE_CURVE ( 'NONE', #25133, #64522, #15390, .T. ) ;
#32493=CARTESIAN_POINT ( 'NONE',  ( -1.374798071107336206, -22.32369649477951512, 11.49999999999999645 ) ) ;
#32496=CARTESIAN_POINT ( 'NONE',  ( -14.29351441246084065, -15.47709782942846424, -1.500000000000002220 ) ) ;
#32497=CARTESIAN_POINT ( 'NONE',  ( -30.53943611156634219, -24.75785870443472447, 8.640462295247353097 ) ) ;
#32498=CARTESIAN_POINT ( 'NONE',  ( 8.914523860536577970, -17.85282776015759154, -1.500000000000002220 ) ) ;
#32499=DIRECTION ( 'NONE',  ( 1.000000000000000000, 3.773278334444166432E-23, 8.201307841325785021E-29 ) ) ;
#32501=CARTESIAN_POINT ( 'NONE',  ( -17.76638496452178018, -13.01238552544781335, -1.500000000000002220 ) ) ;
#32502=CARTESIAN_POINT ( 'NONE',  ( -109.5228709571500616, -29.50248528299804818, 1.056150453629043584 ) ) ;
#32503=VERTEX_POINT ( 'NONE', #30028 ) ;
#32504=CARTESIAN_POINT ( 'NONE',  ( -65.57896135027826290, -24.92592662359561473, 8.075495903017998245 ) ) ;
#32506=CARTESIAN_POINT ( 'NONE',  ( -13.77211689728001964, -15.67653869864640903, 11.49999999999999645 ) ) ;
#32508=CARTESIAN_POINT ( 'NONE',  ( -111.5228709571500616, -23.48786465467242479, 11.44779295918253936 ) ) ;
#32509=CARTESIAN_POINT ( 'NONE',  ( -127.6228709571500559, -23.48783264082479505, -1.443836473390056829 ) ) ;
#32510=CARTESIAN_POINT ( 'NONE',  ( -6.196366259867160942, 20.41550611124569059, 11.49999999999998934 ) ) ;
#32511=LINE ( 'NONE', #41640, #90420 ) ;
#32512=CARTESIAN_POINT ( 'NONE',  ( -66.62287095715005592, -23.47593901973091235, -1.443836447539006196 ) ) ;
#32514=PLANE ( 'NONE',  #42278 ) ;
#32515=LINE ( 'NONE', #55872, #20004 ) ;
#32516=CARTESIAN_POINT ( 'NONE',  ( -21.16606679798846358, 7.723709098063864076, -1.500000000000002220 ) ) ;
#32517=FACE_OUTER_BOUND ( 'NONE', #24620, .T. ) ;
#32518=ORIENTED_EDGE ( 'NONE', *, *, #71035, .T. ) ;
#32520=CARTESIAN_POINT ( 'NONE',  ( -122.6228709571500417, -23.47593901973091235, -1.443836447538997536 ) ) ;
#32521=CARTESIAN_POINT ( 'NONE',  ( 16.13486940644654766, 11.28601765141728741, 11.49999999999999645 ) ) ;
#32522=CARTESIAN_POINT ( 'NONE',  ( -89.52287095715006160, -24.65952944569304606, 1.056160979905700570 ) ) ;
#32525=CARTESIAN_POINT ( 'NONE',  ( -99.59346018923595523, -23.96119346886881374, -0.6495511937831867089 ) ) ;
#32526=CARTESIAN_POINT ( 'NONE',  ( -124.5228709571500616, -29.50248528299804818, 1.056150453629045360 ) ) ;
#32527=PLANE ( 'NONE',  #52870 ) ;
#32530=CARTESIAN_POINT ( 'NONE',  ( -8.281543130087330340, -17.94227898472161797, -1.500000000000002220 ) ) ;
#32532=VERTEX_POINT ( 'NONE', #61001 ) ;
#32533=VECTOR ( 'NONE', #33715, 1000.000000000000114 ) ;
#32534=CARTESIAN_POINT ( 'NONE',  ( -13.29518446780263119, -15.22762515321373478, 11.49999999999999645 ) ) ;
#32535=CARTESIAN_POINT ( 'NONE',  ( -112.6228709571500417, -24.66019654487199730, 8.947790411086124607 ) ) ;
#32536=ADVANCED_FACE ( 'NONE', ( #91935 ), #22406, .T. ) ;
#32538=ORIENTED_EDGE ( 'NONE', *, *, #95128, .T. ) ;
#32539=CARTESIAN_POINT ( 'NONE',  ( -67.62287095715007013, -23.73907113216991860, -1.053371485793226814 ) ) ;
#32540=CARTESIAN_POINT ( 'NONE',  ( -70.04721975296412495, -25.30058798389317332, 5.351639246407742689 ) ) ;
#32541=CARTESIAN_POINT ( 'NONE',  ( -88.88918693012689687, -25.25185156220469551, 6.255794136723666909 ) ) ;
#32542=CARTESIAN_POINT ( 'NONE',  ( -82.62287095715005592, -23.47593901973091235, -1.443836447539004642 ) ) ;
#32543=DIRECTION ( 'NONE',  ( 0.000000000000000000, -0.9999999999976377785, -2.173523156925979128E-06 ) ) ;
#32545=CARTESIAN_POINT ( 'NONE',  ( -10.28607412905329532, -17.16720287211733975, 11.49999999999998934 ) ) ;
#32547=CARTESIAN_POINT ( 'NONE',  ( -116.5534035506147177, -24.35071581493543746, 9.817618358456021710 ) ) ;
#32549=CARTESIAN_POINT ( 'NONE',  ( -104.6228709571500559, -24.66019654487200086, 8.947790411086124607 ) ) ;
#32551=CARTESIAN_POINT ( 'NONE',  ( -35.46596725541123618, -25.00158670708910336, 2.256160236439224143 ) ) ;
#32552=CARTESIAN_POINT ( 'NONE',  ( -82.52287095715006160, -24.64965694238407323, 8.947790433994198267 ) ) ;
#32554=CARTESIAN_POINT ( 'NONE',  ( -83.54433019474268463, -24.51314013834315375, 0.6176544820404104019 ) ) ;
#32556=CARTESIAN_POINT ( 'NONE',  ( -31.62287095715005236, -24.65952944569304250, 1.056160979905689690 ) ) ;
#32557=EDGE_LOOP ( 'NONE', ( #71740, #36862, #84863, #66478 ) ) ;
#32558=CARTESIAN_POINT ( 'NONE',  ( -3.904290608643684379, -19.93223805144805283, 11.49999999999998934 ) ) ;
#32559=CARTESIAN_POINT ( 'NONE',  ( -28.55620429048340370, -24.50151139823071489, 1.056161648317806234 ) ) ;
#32560=CARTESIAN_POINT ( 'NONE',  ( -34.51266535100846511, -23.73766607897670866, -1.055555164236443133 ) ) ;
#32561=CARTESIAN_POINT ( 'NONE',  ( -102.6228709571500559, -29.50250786944525672, 11.44777988621623166 ) ) ;
#32563=EDGE_CURVE ( 'NONE', #69040, #25971, #89276, .T. ) ;
#32565=CARTESIAN_POINT ( 'NONE',  ( 16.36621611169882229, 11.82581248522330064, -1.500000000000002220 ) ) ;
#32566=CARTESIAN_POINT ( 'NONE',  ( 15.93590435955092843, -13.91358336426615239, 11.49999999999999645 ) ) ;
#32567=CARTESIAN_POINT ( 'NONE',  ( -18.17467834739497690, 12.62983929299386965, -1.500000000000002220 ) ) ;
#32568=B_SPLINE_CURVE_WITH_KNOTS ( 'NONE', 3,
 ( #90950, #89955, #68125, #75223 ),
 .UNSPECIFIED., .F., .F.,
 ( 4, 4 ),
 ( 0.000000000000000000, 0.0001000000000000167422 ),
 .UNSPECIFIED. ) ;
#32569=AXIS2_PLACEMENT_3D ( 'NONE', #60495, #4700, #19905 ) ;
#32570=CARTESIAN_POINT ( 'NONE',  ( -20.56140336115741718, 0.6910293267889283664, 11.49999999999998934 ) ) ;
#32571=DIRECTION ( 'NONE',  ( -3.773278334453079618E-23, 0.9999999999976377785, 2.173523156925979975E-06 ) ) ;
#32572=VERTEX_POINT ( 'NONE', #70605 ) ;
#32573=CARTESIAN_POINT ( 'NONE',  ( -94.55620429048339304, -24.66019654487199730, 8.947790411086124607 ) ) ;
#32576=LINE ( 'NONE', #71650, #22657 ) ;
#32577=ORIENTED_EDGE ( 'NONE', *, *, #77412, .F. ) ;
#32581=CARTESIAN_POINT ( 'NONE',  ( -111.4896040003763602, -25.21196470494054509, 3.415743279166374435 ) ) ;
#32584=CARTESIAN_POINT ( 'NONE',  ( 18.97174343470660318, 8.267356841975738391, -1.500000000000002220 ) ) ;
#32585=CARTESIAN_POINT ( 'NONE',  ( 20.17453868081960167, 7.849935799312063089, 11.49999999999999645 ) ) ;
#32587=EDGE_CURVE ( 'NONE', #37822, #68524, #51714, .T. ) ;
#32588=CARTESIAN_POINT ( 'NONE',  ( -98.92106654937062160, -25.27789303035052271, 5.825687011034560214 ) ) ;
#32590=CARTESIAN_POINT ( 'NONE',  ( 15.34105849444754455, 16.31744944422920440, -1.500000000000002220 ) ) ;
#32591=EDGE_CURVE ( 'NONE', #29538, #52807, #39649, .T. ) ;
#32592=CARTESIAN_POINT ( 'NONE',  ( -79.34796103478946350, -25.12205572456604941, 6.000420134665034766 ) ) ;
#32593=CARTESIAN_POINT ( 'NONE',  ( -84.62359692944605172, -24.65952944569303895, 1.056160979905700348 ) ) ;
#32594=ORIENTED_EDGE ( 'NONE', *, *, #36146, .F. ) ;
#32596=VECTOR ( 'NONE', #87059, 1000.000000000000114 ) ;
#32597=CARTESIAN_POINT ( 'NONE',  ( -120.6228709571500417, -24.92604778743018556, 8.074972756849359001 ) ) ;
#32598=ADVANCED_FACE ( 'NONE', ( #40159 ), #77693, .F. ) ;
#32600=VERTEX_POINT ( 'NONE', #46772 ) ;
#32601=EDGE_CURVE ( 'NONE', #91107, #58389, #33476, .T. ) ;
#32603=LINE ( 'NONE', #86390, #19843 ) ;
#32604=EDGE_LOOP ( 'NONE', ( #81797, #61620, #90249, #60437 ) ) ;
#32605=LINE ( 'NONE', #10271, #30915 ) ;
#32606=CARTESIAN_POINT ( 'NONE',  ( 14.70648301983428397, -15.34743991077593250, -1.500000000000002220 ) ) ;
#32608=CARTESIAN_POINT ( 'NONE',  ( -50.60991848927657344, -23.85016227208579309, -0.8807180028928346394 ) ) ;
#32609=CARTESIAN_POINT ( 'NONE',  ( -17.41291239988371231, 13.16847401419012975, -1.500000000000002220 ) ) ;
#32610=CARTESIAN_POINT ( 'NONE',  ( -103.5979546920953993, -23.48786465467241413, 11.44779295918254292 ) ) ;
#32611=CARTESIAN_POINT ( 'NONE',  ( -111.5228709571500616, -24.64898659630368627, 1.056161002820831474 ) ) ;
#32612=CARTESIAN_POINT ( 'NONE',  ( -109.5895376238166961, -24.65952944569304606, 1.056160979905701014 ) ) ;
#32613=CARTESIAN_POINT ( 'NONE',  ( -13.95179422449595208, 16.79422078803934326, -1.500000000000002220 ) ) ;
#32614=CARTESIAN_POINT ( 'NONE',  ( -95.52287095715011844, -24.63287334234179937, 0.9662140553045371894 ) ) ;
#32616=EDGE_CURVE ( 'NONE', #76295, #88312, #79483, .T. ) ;
#32618=CARTESIAN_POINT ( 'NONE',  ( -85.49847897960830778, -24.83644354573578994, 8.397322867130101898 ) ) ;
#32619=ORIENTED_EDGE ( 'NONE', *, *, #67108, .T. ) ;
#32620=VERTEX_POINT ( 'NONE', #78199 ) ;
#32622=FACE_OUTER_BOUND ( 'NONE', #54980, .T. ) ;
#32624=CARTESIAN_POINT ( 'NONE',  ( -21.08002519818654363, -2.465602145356518893, -1.500000000000002220 ) ) ;
#32625=CARTESIAN_POINT ( 'NONE',  ( -94.54934828576006112, -24.34968618360933945, 0.1864209137778860548 ) ) ;
#32626=PLANE ( 'NONE',  #44660 ) ;
#32627=CARTESIAN_POINT ( 'NONE',  ( -44.52287095715006160, -23.48786465467241058, 11.44779295918255180 ) ) ;
#32628=CARTESIAN_POINT ( 'NONE',  ( -127.6228709571500275, -24.66019654487199730, 8.947790411086121054 ) ) ;
#32629=CARTESIAN_POINT ( 'NONE',  ( -4.539579955115475407, -18.87035741768621122, 11.49999999999998934 ) ) ;
#32630=CARTESIAN_POINT ( 'NONE',  ( -45.57314457103787930, -25.00158670708910691, 2.256160236439225031 ) ) ;
#32632=CARTESIAN_POINT ( 'NONE',  ( 4.865394487973861537, 18.91859722749940786, 11.49999999999999645 ) ) ;
#32634=B_SPLINE_CURVE_WITH_KNOTS ( 'NONE', 3,
 ( #10029, #88165, #71947, #87660 ),
 .UNSPECIFIED., .F., .F.,
 ( 4, 4 ),
 ( 2.775557561562891351E-17, 0.001846153846153872347 ),
 .UNSPECIFIED. ) ;
#32637=ORIENTED_EDGE ( 'NONE', *, *, #76248, .T. ) ;
#32639=CARTESIAN_POINT ( 'NONE',  ( -79.62287095715005592, -29.50250786944525672, 11.44777988621623521 ) ) ;
#32640=FACE_OUTER_BOUND ( 'NONE', #66078, .T. ) ;
#32643=CARTESIAN_POINT ( 'NONE',  ( 18.24227566675094181, -7.298356753547692755, -1.500000000000002220 ) ) ;
#32646=CARTESIAN_POINT ( 'NONE',  ( -90.52287095715006160, -24.63345952396256067, 9.038047939301504741 ) ) ;
#32647=FACE_OUTER_BOUND ( 'NONE', #59595, .T. ) ;
#32650=CARTESIAN_POINT ( 'NONE',  ( -125.5228709571500616, -25.00182538069146077, 7.747789668545104647 ) ) ;
#32652=CARTESIAN_POINT ( 'NONE',  ( -76.52287095715003318, -24.34917612406836795, 0.1852690917426554063 ) ) ;
#32653=CARTESIAN_POINT ( 'NONE',  ( -104.5228709571500758, -24.64965694238407323, 8.947790433994194714 ) ) ;
#32655=B_SPLINE_CURVE_WITH_KNOTS ( 'NONE', 3,
 ( #46756, #92411, #68095, #15790, #83805, #99018 ),
 .UNSPECIFIED., .F., .F.,
 ( 4, 2, 4 ),
 ( 0.000000000000000000, 0.001380901958385387677, 0.002761803916770775354 ),
 .UNSPECIFIED. ) ;
#32656=CARTESIAN_POINT ( 'NONE',  ( -129.6235880454576090, -24.34968618360934656, 0.1864209137778921610 ) ) ;
#32657=CARTESIAN_POINT ( 'NONE',  ( -114.5568549121452264, -23.73791477778912196, 11.05961554403169700 ) ) ;
#32658=CARTESIAN_POINT ( 'NONE',  ( -10.02925392579303576, -17.20239368982820238, 11.49999999999998934 ) ) ;
#32659=EDGE_CURVE ( 'NONE', #24865, #43572, #30535, .T. ) ;
#32660=CARTESIAN_POINT ( 'NONE',  ( -75.52207690583590249, -23.48786465467241058, 11.44779295918254824 ) ) ;
#32661=CARTESIAN_POINT ( 'NONE',  ( -19.21288746854601115, 4.878285775029977955, -1.500000000000002220 ) ) ;
#32662=ORIENTED_EDGE ( 'NONE', *, *, #60456, .T. ) ;
#32663=CARTESIAN_POINT ( 'NONE',  ( -122.5228709571500616, -23.72773821059536914, 11.05748984161097326 ) ) ;
#32664=VECTOR ( 'NONE', #28041, 1000.000000000000114 ) ;
#32666=CARTESIAN_POINT ( 'NONE',  ( -51.48549811542276444, -25.22876079287771134, 6.454949072762300233 ) ) ;
#32667=CARTESIAN_POINT ( 'NONE',  ( -92.52287095715006160, -29.50250243563736774, 8.947779886222139822 ) ) ;
#32668=CARTESIAN_POINT ( 'NONE',  ( -20.39401028033356766, -3.670942005906183692, 11.49999999999999645 ) ) ;
#32670=B_SPLINE_CURVE_WITH_KNOTS ( 'NONE', 3,
 ( #61109, #13910, #60616, #12913 ),
 .UNSPECIFIED., .F., .F.,
 ( 4, 4 ),
 ( 0.09056467001404970574, 0.09957110128616525335 ),
 .UNSPECIFIED. ) ;
#32672=CARTESIAN_POINT ( 'NONE',  ( -78.52287095715009002, -24.33927499327854349, 9.819080762295801179 ) ) ;
#32673=CARTESIAN_POINT ( 'NONE',  ( 22.69831151501224298, -1.600861625767590724, 11.49999999999999645 ) ) ;
#32674=EDGE_LOOP ( 'NONE', ( #72007, #41244, #81939, #50832 ) ) ;
#32675=CARTESIAN_POINT ( 'NONE',  ( -69.64018546353763384, -23.96119346886880308, -0.6495511937832122440 ) ) ;
#32677=ORIENTED_EDGE ( 'NONE', *, *, #79220, .F. ) ;
#32678=CARTESIAN_POINT ( 'NONE',  ( -19.95319933381289701, -3.276446921841525306, -1.500000000000002220 ) ) ;
#32680=CARTESIAN_POINT ( 'NONE',  ( -97.62287095715002749, -23.95044443724992078, 10.65354141964649592 ) ) ;
#32681=ORIENTED_EDGE ( 'NONE', *, *, #62771, .T. ) ;
#32683=CARTESIAN_POINT ( 'NONE',  ( -9.034649315346676701, 21.08484869742704504, -1.500000000000002220 ) ) ;
#32685=CARTESIAN_POINT ( 'NONE',  ( 19.98059151383774434, -0.7942727526097331792, -1.500000000000002220 ) ) ;
#32687=CARTESIAN_POINT ( 'NONE',  ( 17.27681320446407298, 11.92757687370068886, 11.49999999999999645 ) ) ;
#32688=CARTESIAN_POINT ( 'NONE',  ( -29.71670104680227453, -25.18823541688493250, 6.230496314888496201 ) ) ;
#32690=CARTESIAN_POINT ( 'NONE',  ( 6.148021820315829444, -21.18842874637755358, -1.500000000000002220 ) ) ;
#32692=EDGE_LOOP ( 'NONE', ( #166, #88318, #19354, #69687 ) ) ;
#32693=VECTOR ( 'NONE', #51718, 1000.000000000000114 ) ;
#32694=DIRECTION ( 'NONE',  ( 0.000000000000000000, -2.173523156925980399E-06, 0.9999999999976378895 ) ) ;
#32695=CARTESIAN_POINT ( 'NONE',  ( -49.52164473449563076, -25.27344882170398321, 3.857971157315336797 ) ) ;
#32696=CARTESIAN_POINT ( 'NONE',  ( -46.62287095715004170, -23.48783264082478439, -1.443836473390070818 ) ) ;
#32697=ORIENTED_EDGE ( 'NONE', *, *, #858, .T. ) ;
#32700=ORIENTED_EDGE ( 'NONE', *, *, #4063, .T. ) ;
#32701=EDGE_CURVE ( 'NONE', #60701, #23124, #49314, .T. ) ;
#32702=FACE_OUTER_BOUND ( 'NONE', #72427, .T. ) ;
#32703=B_SPLINE_CURVE_WITH_KNOTS ( 'NONE', 3,
 ( #84182, #59872, #44636, #60379 ),
 .UNSPECIFIED., .F., .F.,
 ( 4, 4 ),
 ( 0.000000000000000000, 9.999999999999592548E-05 ),
 .UNSPECIFIED. ) ;
#32704=DIRECTION ( 'NONE',  ( 1.000000000000000000, 3.773278334444166432E-23, 8.201307841325785021E-29 ) ) ;
#32705=LINE ( 'NONE', #26096, #146 ) ;
#32706=CARTESIAN_POINT ( 'NONE',  ( 4.814550503181614260, -19.98661186389175271, -1.500000000000002220 ) ) ;
#32708=CARTESIAN_POINT ( 'NONE',  ( -99.38719565547299339, -25.28133435936707585, 5.772806929394654674 ) ) ;
#32709=CARTESIAN_POINT ( 'NONE',  ( -44.59358526570461834, -24.15543982623906416, -0.2315651400026670914 ) ) ;
#32710=CARTESIAN_POINT ( 'NONE',  ( -83.52287095715006160, -24.65952944569304606, 1.056160979905698794 ) ) ;
#32711=CARTESIAN_POINT ( 'NONE',  ( -0.5504121640580519337, 22.28327991085032878, -1.500000000000002220 ) ) ;
#32712=CARTESIAN_POINT ( 'NONE',  ( -0.05081623857416536771, -22.39214385819348507, 8.640809912072072052 ) ) ;
#32713=DIRECTION ( 'NONE',  ( -3.773278334453079030E-23, 0.9999999999976377785, 2.173523156925979128E-06 ) ) ;
#32714=EDGE_LOOP ( 'NONE', ( #40778, #60651, #34888, #83469 ) ) ;
#32715=CARTESIAN_POINT ( 'NONE',  ( -68.62287095715005592, -23.48786465467241058, 11.44779295918254647 ) ) ;
#32716=CARTESIAN_POINT ( 'NONE',  ( -124.6228709571500843, -24.50216790748206108, 0.6166512839542565017 ) ) ;
#32717=EDGE_CURVE ( 'NONE', #41799, #33481, #25026, .T. ) ;
#32718=CARTESIAN_POINT ( 'NONE',  ( -8.730572200882948053, 18.91488879456464289, -1.500000000000002220 ) ) ;
#32724=ORIENTED_EDGE ( 'NONE', *, *, #8136, .T. ) ;
#32725=CARTESIAN_POINT ( 'NONE',  ( -69.21490423241783674, -25.25935235714723959, 7.033986463589522842 ) ) ;
#32726=CARTESIAN_POINT ( 'NONE',  ( -4.359323203648655998, -20.60729432550360585, -1.500000000000002220 ) ) ;
#32729=CARTESIAN_POINT ( 'NONE',  ( -53.52287095715006870, -23.47596703998600631, 11.44779298504229104 ) ) ;
#32731=CARTESIAN_POINT ( 'NONE',  ( -101.6955034991685238, -25.03152311293479571, 6.928826238582348473 ) ) ;
#32732=CARTESIAN_POINT ( 'NONE',  ( -109.9583214895175871, -25.12701665469254664, 2.868629235022660762 ) ) ;
#32733=LINE ( 'NONE', #79405, #28559 ) ;
#32734=CARTESIAN_POINT ( 'NONE',  ( -57.52287095715005449, -24.65952944569304606, 1.056160979905695463 ) ) ;
#32735=CARTESIAN_POINT ( 'NONE',  ( 17.16062296631688255, 14.07911611715085876, 11.49999999999999645 ) ) ;
#32736=ORIENTED_EDGE ( 'NONE', *, *, #38409, .F. ) ;
#32737=EDGE_CURVE ( 'NONE', #45268, #62158, #51641, .T. ) ;
#32740=ORIENTED_EDGE ( 'NONE', *, *, #58743, .F. ) ;
#32741=CARTESIAN_POINT ( 'NONE',  ( -16.57510365746454184, 15.48777146884464884, -1.500000000000002220 ) ) ;
#32742=CARTESIAN_POINT ( 'NONE',  ( -118.6228709571500701, -23.47596703998600631, 11.44779298504227683 ) ) ;
#32743=ORIENTED_EDGE ( 'NONE', *, *, #98921, .T. ) ;
#32745=ORIENTED_EDGE ( 'NONE', *, *, #95204, .T. ) ;
#32748=CARTESIAN_POINT ( 'NONE',  ( 16.24926901856429140, 11.90123039513101411, 11.49999999999998934 ) ) ;
#32749=CARTESIAN_POINT ( 'NONE',  ( -51.52287095715009713, -23.95044443724991723, 10.65354141964648882 ) ) ;
#32750=ORIENTED_EDGE ( 'NONE', *, *, #93546, .F. ) ;
#32751=B_SPLINE_CURVE_WITH_KNOTS ( 'NONE', 3,
 ( #15116, #68906, #90747, #53196 ),
 .UNSPECIFIED., .F., .F.,
 ( 4, 4 ),
 ( 0.000000000000000000, 1.000000000000000000 ),
 .UNSPECIFIED. ) ;
#32752=CARTESIAN_POINT ( 'NONE',  ( -130.5728709571500303, -24.37317526135185375, 9.969885471561841683 ) ) ;
#32753=CARTESIAN_POINT ( 'NONE',  ( 1.926536275058113867, -22.33200895297504474, -1.500000000000002220 ) ) ;
#32756=VERTEX_POINT ( 'NONE', #56905 ) ;
#32757=CARTESIAN_POINT ( 'NONE',  ( -112.6256775209500063, -24.35071581493543391, 9.817618358456018157 ) ) ;
#32759=CARTESIAN_POINT ( 'NONE',  ( -117.6228709571500559, -23.47593901973091235, -1.443836447538997536 ) ) ;
#32763=CARTESIAN_POINT ( 'NONE',  ( -16.94305004876727239, 9.801747318927828800, -1.500000000000002220 ) ) ;
#32764=CARTESIAN_POINT ( 'NONE',  ( -33.62287095715005592, -24.64898659630367206, 1.056161002820817485 ) ) ;
#32766=CARTESIAN_POINT ( 'NONE',  ( -7.189238790567602067, -20.27908067168375794, -1.500000000000002220 ) ) ;
#32767=CARTESIAN_POINT ( 'NONE',  ( -128.5899664415713062, -23.96119346886882084, -0.6495511937831803806 ) ) ;
#32768=CARTESIAN_POINT ( 'NONE',  ( -38.55620429048340014, -23.47593901973091235, -1.443836447539011525 ) ) ;
#32769=CARTESIAN_POINT ( 'NONE',  ( -63.62287095715004881, -24.66019654487199020, 8.947790411086131712 ) ) ;
#32770=B_SPLINE_CURVE_WITH_KNOTS ( 'NONE', 3,
 ( #26935, #41676, #72619, #3116 ),
 .UNSPECIFIED., .F., .F.,
 ( 4, 4 ),
 ( 0.000000000000000000, 0.0001000000000000028644 ),
 .UNSPECIFIED. ) ;
#32771=CARTESIAN_POINT ( 'NONE',  ( -52.62287095715006302, -24.65952944569304250, 1.056160979905695685 ) ) ;
#32772=CARTESIAN_POINT ( 'NONE',  ( 21.75204538223844963, -7.182240389990739438, -1.500000000000002220 ) ) ;
#32774=EDGE_CURVE ( 'NONE', #27745, #59988, #89205, .T. ) ;
#32775=VECTOR ( 'NONE', #23245, 1000.000000000000114 ) ;
#32778=CARTESIAN_POINT ( 'NONE',  ( -89.62287095715004170, -29.50250243563736774, 8.947779886222139822 ) ) ;
#32779=CARTESIAN_POINT ( 'NONE',  ( 4.692034869050136336, 19.47840706813412126, 11.49999999999999645 ) ) ;
#32780=PLANE ( 'NONE',  #26825 ) ;
#32782=CARTESIAN_POINT ( 'NONE',  ( -46.52287095715007581, -23.48783264082477018, -1.443836473390096797 ) ) ;
#32783=CARTESIAN_POINT ( 'NONE',  ( -38.62287095715005592, -24.64965695001467694, 8.947790433994187609 ) ) ;
#32784=CARTESIAN_POINT ( 'NONE',  ( -59.52287095715006160, -29.50248528299804818, 1.056150453629034924 ) ) ;
#32785=CARTESIAN_POINT ( 'NONE',  ( -13.65724274058436194, -16.95215541261048742, -1.500000000000002220 ) ) ;
#32786=CARTESIAN_POINT ( 'NONE',  ( -127.5228709571499763, -23.48783264082477373, -1.443836473390082586 ) ) ;
#32787=CARTESIAN_POINT ( 'NONE',  ( 19.42422255247381457, -2.945173967302487039, -1.500000000000002220 ) ) ;
#32788=FACE_OUTER_BOUND ( 'NONE', #30529, .T. ) ;
#32789=CARTESIAN_POINT ( 'NONE',  ( -32.52287095715008292, -23.94994826722564696, -0.6494450866342749151 ) ) ;
#32792=B_SPLINE_CURVE_WITH_KNOTS ( 'NONE', 3,
 ( #44016, #74948, #83058, #44523 ),
 .UNSPECIFIED., .F., .F.,
 ( 4, 4 ),
 ( 0.000000000000000000, 1.000000000000000000 ),
 .UNSPECIFIED. ) ;
#32795=CARTESIAN_POINT ( 'NONE',  ( 8.954683214801249846, 18.48387022957959047, 11.49999999999999645 ) ) ;
#32797=VECTOR ( 'NONE', #79089, 1000.000000000000114 ) ;
#32800=ADVANCED_FACE ( 'NONE', ( #64028 ), #94943, .T. ) ;
#32801=CARTESIAN_POINT ( 'NONE',  ( 22.57354875331468591, -1.174960877787051716, 11.49999999999999645 ) ) ;
#32804=CARTESIAN_POINT ( 'NONE',  ( -69.86129607977629519, -25.12219122924749826, 7.001236562355686921 ) ) ;
#32805=CARTESIAN_POINT ( 'NONE',  ( -26.95182783290497852, -24.79956601504498437, 7.385977329265138280 ) ) ;
#32807=CARTESIAN_POINT ( 'NONE',  ( -74.92287095715006728, -23.47593901973090524, -1.443836447538997980 ) ) ;
#32809=CARTESIAN_POINT ( 'NONE',  ( -69.52287095715006160, -29.50248528299804818, 1.056150453629036701 ) ) ;
#32811=ADVANCED_FACE ( 'NONE', ( #96945 ), #79713, .T. ) ;
#32812=ORIENTED_EDGE ( 'NONE', *, *, #81393, .T. ) ;
#32815=CARTESIAN_POINT ( 'NONE',  ( -2.521034868938843765, 22.70145277337256218, 11.49999999999998934 ) ) ;
#32817=CARTESIAN_POINT ( 'NONE',  ( -65.62287095715005592, -29.50250786944525672, 11.44777988621623699 ) ) ;
#32820=CARTESIAN_POINT ( 'NONE',  ( 9.993301969596378953, 20.15287186522775542, 11.49999999999999645 ) ) ;
#32822=CARTESIAN_POINT ( 'NONE',  ( -38.62287095715005592, -23.47596703998600276, 11.44779298504227505 ) ) ;
#32823=CARTESIAN_POINT ( 'NONE',  ( -12.87221125579857528, -17.80329210173279364, 11.49999999999998934 ) ) ;
#32825=CARTESIAN_POINT ( 'NONE',  ( -44.64704844554334784, -23.96169478059712787, 10.65365249895718414 ) ) ;
#32826=CARTESIAN_POINT ( 'NONE',  ( -56.62287095715005592, -23.48786465467241413, 11.44779295918254824 ) ) ;
#32828=ORIENTED_EDGE ( 'NONE', *, *, #96034, .F. ) ;
#32830=CARTESIAN_POINT ( 'NONE',  ( -41.62287095715006302, -29.50248528299804818, 1.056150453629031594 ) ) ;
#32831=ORIENTED_EDGE ( 'NONE', *, *, #18729, .T. ) ;
#32832=CARTESIAN_POINT ( 'NONE',  ( -19.82921842031888104, 5.099586017421429140, 11.49999999999998934 ) ) ;
#32833=ORIENTED_EDGE ( 'NONE', *, *, #59185, .T. ) ;
#32834=ORIENTED_EDGE ( 'NONE', *, *, #12946, .F. ) ;
#32835=AXIS2_PLACEMENT_3D ( 'NONE', #46835, #77753, #8267 ) ;
#32837=ORIENTED_EDGE ( 'NONE', *, *, #50963, .T. ) ;
#32838=EDGE_CURVE ( 'NONE', #14217, #31069, #54166, .T. ) ;
#32839=CARTESIAN_POINT ( 'NONE',  ( 16.03631736716203449, -16.64276770305488284, -1.500000000000002220 ) ) ;
#32840=CARTESIAN_POINT ( 'NONE',  ( -39.43510301730458423, -25.26871255744266875, 3.880430150159563940 ) ) ;
#32841=CARTESIAN_POINT ( 'NONE',  ( -0.9335293527496063559, -20.33857301660709638, -1.500000000000002220 ) ) ;
#32842=EDGE_LOOP ( 'NONE', ( #34543, #99734, #85633, #4315 ) ) ;
#32843=LINE ( 'NONE', #63820, #86591 ) ;
#32846=CARTESIAN_POINT ( 'NONE',  ( -78.62287095715004170, -24.65952944569304606, 1.056160979905698349 ) ) ;
#32848=CARTESIAN_POINT ( 'NONE',  ( 20.96596170256846747, -4.772324250704091497, 11.49999999999999645 ) ) ;
#32850=CARTESIAN_POINT ( 'NONE',  ( -75.49753373454176142, -24.63355581998385802, 0.9682620441943947664 ) ) ;
#32853=CARTESIAN_POINT ( 'NONE',  ( -10.32638548400381673, 17.97674989526738898, 11.49999999999998934 ) ) ;
#32854=EDGE_CURVE ( 'NONE', #13179, #2429, #38324, .T. ) ;
#32859=B_SPLINE_SURFACE_WITH_KNOTS ( 'NONE', 3, 1, ( 
 ( #83261, #28473 ),
 ( #90876, #45213 ),
 ( #30476, #20351 ),
 ( #59439, #29466 ),
 ( #76139, #76633 ),
 ( #13740, #36587 ),
 ( #20856, #43713 ),
 ( #37592, #52325 ),
 ( #60451, #82761 ),
 ( #51830, #13242 ),
 ( #75149, #6636 ),
 ( #74648, #91371 ),
 ( #5639, #21847 ),
 ( #52821, #68542 ),
 ( #99475, #14742 ),
 ( #82266, #45707 ),
 ( #23346, #9138 ),
 ( #2047, #8648 ),
 ( #24860, #38590 ) ),
 .UNSPECIFIED., .F., .F., .F.,
 ( 4, 1, 1, 1, 1, 1, 1, 1, 1, 1, 1, 1, 1, 1, 1, 1, 4 ),
 ( 2, 2 ),
 ( 0.000000000000000000, 0.05456394950705841657, 0.1078262027811427159, 0.1619237085214018657, 0.2175097010530381569, 0.2744983327961385555, 0.3348147646240177133, 0.3975549470643523486, 0.4647545773561987947, 0.5329012097695247085, 0.6000972138233301445, 0.6653541614565452456, 0.7310836277242112047, 0.7968834939590061506, 0.8632915901470210596, 0.9308312175092489094, 0.9999999999999998890 ),
 ( 0.000000000000000000, 1.000000000000000000 ),
 .UNSPECIFIED. ) ;
#32861=CARTESIAN_POINT ( 'NONE',  ( -82.52287095715006160, -24.64898659630367916, 1.056161002820826145 ) ) ;
#32862=DIRECTION ( 'NONE',  ( -3.773278334453079618E-23, 0.9999999999976377785, 2.173523156925979975E-06 ) ) ;
#32864=ORIENTED_EDGE ( 'NONE', *, *, #45108, .F. ) ;
#32866=CARTESIAN_POINT ( 'NONE',  ( -42.49244915491595975, -24.35071581493542681, 9.817618358456037697 ) ) ;
#32868=CARTESIAN_POINT ( 'NONE',  ( 21.11370014442628218, -6.196533921283487345, 11.49999999999999645 ) ) ;
#32871=CARTESIAN_POINT ( 'NONE',  ( -103.5195659409635454, -23.73766607897670156, -1.055555164236454901 ) ) ;
#32873=CARTESIAN_POINT ( 'NONE',  ( -14.53490578827140212, -17.26895500059623956, -1.500000000000002220 ) ) ;
#32874=CARTESIAN_POINT ( 'NONE',  ( 20.92198360912786015, -1.804805560479522342, -1.500000000000002220 ) ) ;
#32875=EDGE_CURVE ( 'NONE', #65785, #85381, #35998, .T. ) ;
#32878=VECTOR ( 'NONE', #53516, 1000.000000000000114 ) ;
#32879=ORIENTED_EDGE ( 'NONE', *, *, #58494, .T. ) ;
#32880=CARTESIAN_POINT ( 'NONE',  ( -58.62287095715004881, -23.48786465467241769, 11.44779295918254824 ) ) ;
#32882=ORIENTED_EDGE ( 'NONE', *, *, #30426, .F. ) ;
#32883=CARTESIAN_POINT ( 'NONE',  ( 19.97935793590388442, -6.945280299276400449, 11.49999999999998934 ) ) ;
#32885=CARTESIAN_POINT ( 'NONE',  ( -58.85737199502123929, -25.27183489919805126, 3.712349809207164952 ) ) ;
#32886=CARTESIAN_POINT ( 'NONE',  ( -121.5564787168670051, -23.73766607897670866, -1.055555164236450905 ) ) ;
#32889=CARTESIAN_POINT ( 'NONE',  ( 21.63176498729014341, 4.993826359924048219, -1.500000000000002220 ) ) ;
#32890=CARTESIAN_POINT ( 'NONE',  ( -114.5945979628053948, -23.48783264082478794, -1.443836473390062380 ) ) ;
#32891=ORIENTED_EDGE ( 'NONE', *, *, #64031, .F. ) ;
#32893=CARTESIAN_POINT ( 'NONE',  ( -64.62287095715007013, -24.50321055353804311, 9.387540953477527594 ) ) ;
#32894=CARTESIAN_POINT ( 'NONE',  ( -126.6248978461467516, -23.73766607897670156, -1.055555164236450016 ) ) ;
#32895=CARTESIAN_POINT ( 'NONE',  ( -40.43756433397305727, -25.11033443737753501, 2.832404817301930056 ) ) ;
#32898=EDGE_CURVE ( 'NONE', #19646, #60374, #72621, .T. ) ;
#32899=CARTESIAN_POINT ( 'NONE',  ( -15.31790942089943286, 12.02624123284522106, -1.500000000000002220 ) ) ;
#32901=CARTESIAN_POINT ( 'NONE',  ( 1.185105815240312888, -21.37944065014308848, 11.49999999999998934 ) ) ;
#32903=CARTESIAN_POINT ( 'NONE',  ( -100.6228709571500417, -24.15516710230295061, 10.28746687063725673 ) ) ;
#32904=CARTESIAN_POINT ( 'NONE',  ( -77.58473169878783438, -24.51314013834315375, 0.6176544820404131775 ) ) ;
#32905=CARTESIAN_POINT ( 'NONE',  ( 21.64774270073068863, 7.000884456547583845, -1.500000000000002220 ) ) ;
#32906=AXIS2_PLACEMENT_3D ( 'NONE', #6457, #60757, #22160 ) ;
#32907=CARTESIAN_POINT ( 'NONE',  ( -102.6335671968240177, -23.73766607897671932, -1.055555164236430477 ) ) ;
#32908=CARTESIAN_POINT ( 'NONE',  ( -95.62287095715005592, -29.50250243563736774, 8.947779886222138046 ) ) ;
#32909=CARTESIAN_POINT ( 'NONE',  ( 18.78741845327603599, -6.401996767227196905, 11.49999999999999645 ) ) ;
#32910=CARTESIAN_POINT ( 'NONE',  ( -123.5542511647627322, -24.51419770103158768, 9.386484678747160970 ) ) ;
#32913=FACE_OUTER_BOUND ( 'NONE', #29341, .T. ) ;
#32917=CARTESIAN_POINT ( 'NONE',  ( -71.52287095715007581, -23.47596703998600631, 11.44779298504228748 ) ) ;
#32918=CARTESIAN_POINT ( 'NONE',  ( 4.495418090846292181, 21.21921847905042569, -1.500000000000002220 ) ) ;
#32919=CARTESIAN_POINT ( 'NONE',  ( -56.64375666506161622, -23.96169478059713498, 10.65365249895718236 ) ) ;
#32920=CARTESIAN_POINT ( 'NONE',  ( -8.384790838521158918, 17.58144419890746235, -1.500000000000002220 ) ) ;
#32921=LINE ( 'NONE', #62891, #94456 ) ;
#32922=ORIENTED_EDGE ( 'NONE', *, *, #43712, .F. ) ;
#32923=CARTESIAN_POINT ( 'NONE',  ( -5.688044216684545518, -19.60349290560521140, 11.49999999999999645 ) ) ;
#32928=CARTESIAN_POINT ( 'NONE',  ( -41.43253813893231552, -25.26941562057272606, 3.941780839177481788 ) ) ;
#32930=CARTESIAN_POINT ( 'NONE',  ( -76.52287095715007581, -24.65952944569304606, 1.056160979905698794 ) ) ;
#32935=VERTEX_POINT ( 'NONE', #29419 ) ;
#32939=EDGE_CURVE ( 'NONE', #78152, #64814, #52272, .T. ) ;
#32940=CARTESIAN_POINT ( 'NONE',  ( 6.461317529299694051, 22.01590093704556850, 11.49999999999999645 ) ) ;
#32941=CARTESIAN_POINT ( 'NONE',  ( -4.508144621425604903, 22.28865971958312997, -1.500000000000002220 ) ) ;
#32943=CARTESIAN_POINT ( 'NONE',  ( -119.5228709571500616, -23.48783264082477018, -1.443836473390082142 ) ) ;
#32944=VECTOR ( 'NONE', #54026, 1000.000000000000114 ) ;
#32945=DIRECTION ( 'NONE',  ( -3.773278334453079618E-23, 0.9999999999976377785, 2.173523156925979975E-06 ) ) ;
#32946=CARTESIAN_POINT ( 'NONE',  ( -90.64712176407903144, -23.48783264082477018, -1.443836473390091912 ) ) ;
#32949=CARTESIAN_POINT ( 'NONE',  ( -69.54083733670222500, -24.51419770103157347, 9.386484678747178734 ) ) ;
#32950=CARTESIAN_POINT ( 'NONE',  ( -26.13079664625181309, -24.93797848278802576, 4.224548870800117761 ) ) ;
#32951=CARTESIAN_POINT ( 'NONE',  ( -90.52287095715009002, -23.48783264082477373, -1.443836473390088582 ) ) ;
#32954=CARTESIAN_POINT ( 'NONE',  ( -9.549598871097368047, 18.00506641634745009, 11.49999999999998934 ) ) ;
#32955=ORIENTED_EDGE ( 'NONE', *, *, #62733, .F. ) ;
#32956=EDGE_LOOP ( 'NONE', ( #75898, #61590, #62534, #96893 ) ) ;
#32957=EDGE_CURVE ( 'NONE', #6738, #37215, #52894, .T. ) ;
#32958=CARTESIAN_POINT ( 'NONE',  ( -15.77545706029219730, -16.76941864122914083, 11.49999999999998934 ) ) ;
#32960=ORIENTED_EDGE ( 'NONE', *, *, #42529, .T. ) ;
#32963=AXIS2_PLACEMENT_3D ( 'NONE', #27311, #3983, #73988 ) ;
#32965=CARTESIAN_POINT ( 'NONE',  ( -58.87764846857956513, -25.14083923594470704, 2.947789366366647901 ) ) ;
#32966=FACE_OUTER_BOUND ( 'NONE', #50811, .T. ) ;
#32967=CARTESIAN_POINT ( 'NONE',  ( -18.01091527469349529, -11.40912366963296698, 11.49999999999999645 ) ) ;
#32969=ORIENTED_EDGE ( 'NONE', *, *, #24180, .F. ) ;
#32970=CARTESIAN_POINT ( 'NONE',  ( 6.060481786824854389, 21.40074245971799627, 11.49999999999998934 ) ) ;
#32971=CARTESIAN_POINT ( 'NONE',  ( -15.52656095410427817, -13.64048245868121434, 11.49999999999998934 ) ) ;
#32972=EDGE_CURVE ( 'NONE', #29423, #40078, #4567, .T. ) ;
#32974=VERTEX_POINT ( 'NONE', #20300 ) ;
#32976=FACE_BOUND ( 'NONE', #61444, .T. ) ;
#32978=CARTESIAN_POINT ( 'NONE',  ( -79.55620429048337883, -23.48786465467241058, 11.44779295918254469 ) ) ;
#32979=ORIENTED_EDGE ( 'NONE', *, *, #94823, .F. ) ;
#32980=VECTOR ( 'NONE', #1188, 1000.000000000000114 ) ;
#32981=CARTESIAN_POINT ( 'NONE',  ( -58.58749944175303170, -24.35071581493543036, 9.817618358456028815 ) ) ;
#32983=CARTESIAN_POINT ( 'NONE',  ( -2.238888094254589234, -20.74146561784671761, -1.500000000000002220 ) ) ;
#32984=CARTESIAN_POINT ( 'NONE',  ( 16.27406392464308027, 14.57352745747340172, 11.49999999999999645 ) ) ;
#32986=CARTESIAN_POINT ( 'NONE',  ( -73.63047128846197609, -24.35071581493543036, 9.817618358456027039 ) ) ;
#32988=CARTESIAN_POINT ( 'NONE',  ( -20.52357230491503159, 9.176553703681571861, 11.49999999999998934 ) ) ;
#32990=CARTESIAN_POINT ( 'NONE',  ( -118.5222382631839650, -23.48786465467241769, 11.44779295918253581 ) ) ;
#32993=ORIENTED_EDGE ( 'NONE', *, *, #95965, .T. ) ;
#32994=VERTEX_POINT ( 'NONE', #29922 ) ;
#32995=ORIENTED_EDGE ( 'NONE', *, *, #19735, .T. ) ;
#32998=CARTESIAN_POINT ( 'NONE',  ( 16.75108703964928480, -13.32659110743468212, -1.500000000000002220 ) ) ;
#32999=CARTESIAN_POINT ( 'NONE',  ( -19.80502325505778671, 10.42642913751328670, 11.49999999999999645 ) ) ;
#33000=ORIENTED_EDGE ( 'NONE', *, *, #5717, .T. ) ;
#33001=CARTESIAN_POINT ( 'NONE',  ( -68.55620429048339304, -24.65952944569304606, 1.056160979905698794 ) ) ;
#33002=CARTESIAN_POINT ( 'NONE',  ( 17.02745815656931683, -12.38318283856952107, -1.500000000000002220 ) ) ;
#33003=CARTESIAN_POINT ( 'NONE',  ( -30.52452761580430263, -25.14647750993875519, 7.291421475381018702 ) ) ;
#33004=CARTESIAN_POINT ( 'NONE',  ( -11.57717615966994273, 16.22069937712612031, -1.500000000000002220 ) ) ;
#33005=CARTESIAN_POINT ( 'NONE',  ( -123.5228709571500616, -29.50248528299804818, 1.056150453629045360 ) ) ;
#33006=CARTESIAN_POINT ( 'NONE',  ( -80.61306835763387824, -25.30877077354806914, 4.525992615401982277 ) ) ;
#33007=CARTESIAN_POINT ( 'NONE',  ( 18.76863814860013235, 11.56883167669432133, -1.500000000000002220 ) ) ;
#33008=VERTEX_POINT ( 'NONE', #44659 ) ;
#33009=CARTESIAN_POINT ( 'NONE',  ( -65.53967300336732649, -24.63419186844611275, 9.035850630976918652 ) ) ;
#33011=FACE_OUTER_BOUND ( 'NONE', #97005, .T. ) ;
#33012=CARTESIAN_POINT ( 'NONE',  ( -20.82246440549779720, 1.468558417816581807, 11.49999999999999645 ) ) ;
#33014=VECTOR ( 'NONE', #95227, 1000.000000000000114 ) ;
#33015=DIRECTION ( 'NONE',  ( 0.000000000000000000, -0.9999999999976377785, -2.173523156925979975E-06 ) ) ;
#33016=CARTESIAN_POINT ( 'NONE',  ( -127.5562042904834215, -23.48783264082479505, -1.443836473390056829 ) ) ;
#33017=CARTESIAN_POINT ( 'NONE',  ( -21.31669061289120037, -0.5855882196083471714, -1.500000000000002220 ) ) ;
#33018=CARTESIAN_POINT ( 'NONE',  ( -104.5228709571500758, -24.66019654487200441, 8.947790411086113949 ) ) ;
#33019=CARTESIAN_POINT ( 'NONE',  ( -50.81798825283360799, -25.20438501375636875, 3.361021725245152858 ) ) ;
#33020=CARTESIAN_POINT ( 'NONE',  ( -31.62287095715005236, -23.47596703998600276, 11.44779298504227505 ) ) ;
#33021=CARTESIAN_POINT ( 'NONE',  ( -69.99162906124911387, -25.30188801935125653, 5.302352381037461093 ) ) ;
#33022=CARTESIAN_POINT ( 'NONE',  ( -17.80605238980536953, 13.89162706601689479, -1.500000000000002220 ) ) ;
#33023=CARTESIAN_POINT ( 'NONE',  ( -123.5895376238167245, -24.64898659630368627, 1.056161002820393158 ) ) ;
#33026=CARTESIAN_POINT ( 'NONE',  ( -31.65061454106520600, -23.96169478059712432, 10.65365249895719124 ) ) ;
#33027=CARTESIAN_POINT ( 'NONE',  ( 9.442166470422634461, 17.27452087139410963, 11.49999999999999645 ) ) ;
#33029=FACE_OUTER_BOUND ( 'NONE', #51558, .T. ) ;
#33030=VERTEX_POINT ( 'NONE', #89337 ) ;
#33031=CARTESIAN_POINT ( 'NONE',  ( -56.52287095715006870, -24.64898659630367916, 1.056161002820822592 ) ) ;
#33032=CARTESIAN_POINT ( 'NONE',  ( -83.62287095715007013, -23.48786465467241769, 11.44779295918254469 ) ) ;
#33035=CARTESIAN_POINT ( 'NONE',  ( -81.62287095715005592, -29.50250243563736774, 8.947779886222141599 ) ) ;
#33037=CARTESIAN_POINT ( 'NONE',  ( 17.61170953066113398, -8.936083093766256980, 11.49999999999998934 ) ) ;
#33038=ORIENTED_EDGE ( 'NONE', *, *, #5033, .F. ) ;
#33039=CARTESIAN_POINT ( 'NONE',  ( -11.13811422090317294, 16.88724661786912762, 11.49999999999999645 ) ) ;
#33040=CARTESIAN_POINT ( 'NONE',  ( -112.6228709571500275, -24.51387760970725083, 9.387446482453412955 ) ) ;
#33042=EDGE_LOOP ( 'NONE', ( #12736, #39353, #27115, #75126 ) ) ;
#33043=CARTESIAN_POINT ( 'NONE',  ( -110.6228709571500701, -23.48783264082479505, -1.443836473390060160 ) ) ;
#33044=CARTESIAN_POINT ( 'NONE',  ( -69.34448478228789270, -25.25183673717061694, 6.146172466399267620 ) ) ;
#33045=CARTESIAN_POINT ( 'NONE',  ( -51.46011314183329688, -25.27661340440378623, 5.843653433976077949 ) ) ;
#33046=DIRECTION ( 'NONE',  ( 0.000000000000000000, 0.9999999999976377785, 2.173523156925979128E-06 ) ) ;
#33047=EDGE_CURVE ( 'NONE', #48489, #60457, #44458, .T. ) ;
#33049=AXIS2_PLACEMENT_3D ( 'NONE', #75056, #28390, #5557 ) ;
#33051=B_SPLINE_CURVE_WITH_KNOTS ( 'NONE', 3,
 ( #36665, #29047, #60022, #90949 ),
 .UNSPECIFIED., .F., .F.,
 ( 4, 4 ),
 ( 0.000000000000000000, 0.0001002978970080628312 ),
 .UNSPECIFIED. ) ;
#33052=CARTESIAN_POINT ( 'NONE',  ( -96.52287095715004739, -23.96127896941631974, -0.6493128931037976947 ) ) ;
#33053=CARTESIAN_POINT ( 'NONE',  ( -1.591348192139008466, -19.94584644712825039, -1.500000000000002220 ) ) ;
#33054=EDGE_CURVE ( 'NONE', #45090, #37127, #62605, .T. ) ;
#33056=CARTESIAN_POINT ( 'NONE',  ( -116.5196406133853628, -23.96169478059713853, 10.65365249895717348 ) ) ;
#33060=CARTESIAN_POINT ( 'NONE',  ( -79.54043201964276477, -24.66019654487199375, 8.947790411086119278 ) ) ;
#33061=CARTESIAN_POINT ( 'NONE',  ( -35.48816746163671354, -24.40034930558991277, 0.3402023900116170063 ) ) ;
#33062=CARTESIAN_POINT ( 'NONE',  ( -79.88885947674448573, -25.30549239610902390, 5.065442659042057372 ) ) ;
#33064=CARTESIAN_POINT ( 'NONE',  ( -84.62287095715005592, -29.50247984919015209, -1.443849546365053582 ) ) ;
#33065=B_SPLINE_CURVE_WITH_KNOTS ( 'NONE', 3,
 ( #78011, #40478, #8523, #71431, #94752, #39969, #79529, #39473 ),
 .UNSPECIFIED., .F., .F.,
 ( 4, 2, 2, 4 ),
 ( 6.384118678600685898E-06, 0.002007151183507250615, 0.003007534715921577739, 0.004007918248335903995 ),
 .UNSPECIFIED. ) ;
#33067=CARTESIAN_POINT ( 'NONE',  ( -49.88931575556473064, -25.19893203316160779, 3.394471111229040883 ) ) ;
#33069=CARTESIAN_POINT ( 'NONE',  ( 19.35245777310151993, -6.127589836641541332, 11.49999999999998934 ) ) ;
#33071=CARTESIAN_POINT ( 'NONE',  ( -34.47821653490140648, -24.65952944569304606, 1.056160979905694353 ) ) ;
#33072=CARTESIAN_POINT ( 'NONE',  ( -107.5228709571500900, -24.51387760970725793, 9.387446482453409402 ) ) ;
#33073=VERTEX_POINT ( 'NONE', #93313 ) ;
#33074=CARTESIAN_POINT ( 'NONE',  ( -83.52287095715006160, -23.48786465467241769, 11.44779295918254469 ) ) ;
#33075=EDGE_CURVE ( 'NONE', #68625, #73282, #40856, .T. ) ;
#33076=AXIS2_PLACEMENT_3D ( 'NONE', #22564, #44444, #68275 ) ;
#33077=CARTESIAN_POINT ( 'NONE',  ( -14.54676392617323266, -15.37779485849079464, 11.49999999999999645 ) ) ;
#33078=CARTESIAN_POINT ( 'NONE',  ( 22.15222936869060177, 0.07132910108538677296, -1.500000000000002220 ) ) ;
#33079=CARTESIAN_POINT ( 'NONE',  ( 18.12345787009687115, -9.690629616749632191, 11.49999999999998934 ) ) ;
#33081=DIRECTION ( 'NONE',  ( 0.000000000000000000, 2.173523156925980399E-06, -0.9999999999976378895 ) ) ;
#33082=ORIENTED_EDGE ( 'NONE', *, *, #9310, .T. ) ;
#33083=CARTESIAN_POINT ( 'NONE',  ( -54.58739168452969892, -24.34968618360932879, 0.1864209137778771175 ) ) ;
#33084=CARTESIAN_POINT ( 'NONE',  ( -85.92287095715006728, -23.47593901973090169, -1.443836447538997092 ) ) ;
#33088=CARTESIAN_POINT ( 'NONE',  ( -112.6228709571500417, -24.51283580621365843, 0.6167428607019777020 ) ) ;
#33091=CARTESIAN_POINT ( 'NONE',  ( 18.79598114143782084, -8.675585332008726169, -1.500000000000002220 ) ) ;
#33092=CARTESIAN_POINT ( 'NONE',  ( 2.186256072416925544, -21.55203199515037582, 11.49999999999999645 ) ) ;
#33093=ORIENTED_EDGE ( 'NONE', *, *, #41956, .T. ) ;
#33094=CARTESIAN_POINT ( 'NONE',  ( -60.52287095715006160, -23.48786465467241058, 11.44779295918254824 ) ) ;
#33095=DIRECTION ( 'NONE',  ( -3.773278334453079618E-23, 0.9999999999976377785, 2.173523156925979975E-06 ) ) ;
#33096=CARTESIAN_POINT ( 'NONE',  ( 18.65981798208652265, 12.38953945867474360, -1.500000000000002220 ) ) ;
#33098=DIRECTION ( 'NONE',  ( 3.773278334444167608E-23, -1.000000000000000000, 0.000000000000000000 ) ) ;
#33102=CARTESIAN_POINT ( 'NONE',  ( -100.5228709571500900, -23.48783264082477018, -1.443836473390086583 ) ) ;
#33104=ORIENTED_EDGE ( 'NONE', *, *, #53083, .T. ) ;
#33105=EDGE_CURVE ( 'NONE', #40854, #46960, #1490, .T. ) ;
#33106=DIRECTION ( 'NONE',  ( -3.773278334453079618E-23, 0.9999999999976377785, 2.173523156925979975E-06 ) ) ;
#33107=EDGE_LOOP ( 'NONE', ( #12325, #20356, #35249, #97269 ) ) ;
#33109=CARTESIAN_POINT ( 'NONE',  ( -3.247986963444697395, 20.98610878802851332, -1.500000000000002220 ) ) ;
#33110=VERTEX_POINT ( 'NONE', #61393 ) ;
#33111=CARTESIAN_POINT ( 'NONE',  ( -50.63203686936204662, -24.73486907724918282, 1.287355809206965684 ) ) ;
#33112=CARTESIAN_POINT ( 'NONE',  ( -19.95566455537076678, 8.849265345510103131, 11.49999999999998934 ) ) ;
#33113=CARTESIAN_POINT ( 'NONE',  ( -52.59321787669466630, -24.15620529776627734, 10.23563542870661003 ) ) ;
#33114=CARTESIAN_POINT ( 'NONE',  ( -107.5228709571500616, -24.33832256527048798, 0.1851278514138657294 ) ) ;
#33115=FACE_OUTER_BOUND ( 'NONE', #67545, .T. ) ;
#33116=CARTESIAN_POINT ( 'NONE',  ( 12.66425630052701479, 17.85959152241435177, -1.500000000000002220 ) ) ;
#33117=CARTESIAN_POINT ( 'NONE',  ( -30.57287095715006942, -24.99131595220528368, 7.800444815679671073 ) ) ;
#33120=CARTESIAN_POINT ( 'NONE',  ( -85.54876333844239866, -24.40133493613049964, 9.663955038902802386 ) ) ;
#33121=EDGE_LOOP ( 'NONE', ( #11369, #28877, #5185, #69294 ) ) ;
#33123=ORIENTED_EDGE ( 'NONE', *, *, #27924, .F. ) ;
#33124=LINE ( 'NONE', #85911, #92912 ) ;
#33126=CARTESIAN_POINT ( 'NONE',  ( -17.82860346875387947, 11.52481846644873187, 11.49999999999998934 ) ) ;
#33132=CARTESIAN_POINT ( 'NONE',  ( 15.36829964806744364, -11.83880051060199712, 11.49999999999998934 ) ) ;
#33133=CARTESIAN_POINT ( 'NONE',  ( -45.48769855799984896, -24.52300882791528380, 0.6510814631126234930 ) ) ;
#33134=ORIENTED_EDGE ( 'NONE', *, *, #37851, .T. ) ;
#33135=CARTESIAN_POINT ( 'NONE',  ( -1.081029368968937421, 19.50181592447522050, 11.49999999999999645 ) ) ;
#33137=CARTESIAN_POINT ( 'NONE',  ( -107.5562042904834072, -24.65952944569304961, 1.056160979905703456 ) ) ;
#33141=CARTESIAN_POINT ( 'NONE',  ( -119.5228709571500758, -24.64965694238408034, 8.947790433994191162 ) ) ;
#33143=CARTESIAN_POINT ( 'NONE',  ( -80.77473702827948898, -25.24813986770818630, 7.542257150238226515 ) ) ;
#33144=CARTESIAN_POINT ( 'NONE',  ( 14.19269941865516671, -13.59168563846684563, -1.500000000000002220 ) ) ;
#33146=DIRECTION ( 'NONE',  ( 3.773278334444167608E-23, -1.000000000000000000, 0.000000000000000000 ) ) ;
#33147=CARTESIAN_POINT ( 'NONE',  ( 8.286623624103266097E-13, -23.05000000000000426, -1.500000000000002220 ) ) ;
#33151=CARTESIAN_POINT ( 'NONE',  ( -40.52287095715005449, -29.50249982740957577, 7.747779886224967605 ) ) ;
#33152=LINE ( 'NONE', #48897, #47697 ) ;
#33153=CARTESIAN_POINT ( 'NONE',  ( -81.90251867898965088, -25.27183487616304447, 3.712349674769177987 ) ) ;
#33155=PLANE ( 'NONE',  #87917 ) ;
#33156=CARTESIAN_POINT ( 'NONE',  ( -73.52287095715004739, -24.35013146730203815, 9.818937971375099494 ) ) ;
#33157=CARTESIAN_POINT ( 'NONE',  ( -48.87380231474225667, -25.25252557466923520, 6.137092008254006359 ) ) ;
#33158=CARTESIAN_POINT ( 'NONE',  ( -10.29545327866581950, 17.06371652956568852, -1.500000000000002220 ) ) ;
#33159=EDGE_CURVE ( 'NONE', #53307, #67032, #24311, .T. ) ;
#33160=DIRECTION ( 'NONE',  ( 3.773278334444166432E-23, -1.000000000000000000, 0.000000000000000000 ) ) ;
#33161=CARTESIAN_POINT ( 'NONE',  ( 1.822157996128044299, -19.77364354024053839, -1.500000000000002220 ) ) ;
#33163=DIRECTION ( 'NONE',  ( 0.000000000000000000, 0.9999999999976377785, 2.173523156925979975E-06 ) ) ;
#33164=ADVANCED_FACE ( 'NONE', ( #53274 ), #43475, .T. ) ;
#33165=ADVANCED_FACE ( 'NONE', ( #49174 ), #95821, .F. ) ;
#33167=VECTOR ( 'NONE', #84253, 1000.000000000000114 ) ;
#33168=CARTESIAN_POINT ( 'NONE',  ( -42.62287095715004881, -24.64965695001467694, 8.947790433994187609 ) ) ;
#33169=CARTESIAN_POINT ( 'NONE',  ( -2.730994233912177549, 20.60462238790213618, 11.49999999999999645 ) ) ;
#33170=CARTESIAN_POINT ( 'NONE',  ( -81.64591219847839909, -23.48783264082478084, -1.443836473390067043 ) ) ;
#33171=EDGE_CURVE ( 'NONE', #5284, #60317, #63897, .T. ) ;
#33172=DIRECTION ( 'NONE',  ( -3.773278334453080206E-23, 0.9999999999976377785, 2.173523156925979975E-06 ) ) ;
#33173=CARTESIAN_POINT ( 'NONE',  ( -9.359374538088376383, 20.77767741201286711, 11.49999999999999645 ) ) ;
#33175=CARTESIAN_POINT ( 'NONE',  ( -112.5228709571500616, -23.47596703998600631, 11.44779298504228038 ) ) ;
#33178=CARTESIAN_POINT ( 'NONE',  ( -20.14672940031187665, -1.731937678239350298, 11.49999999999998934 ) ) ;
#33180=CARTESIAN_POINT ( 'NONE',  ( -106.5228709571501327, -24.35013146730203815, 9.818937971375095941 ) ) ;
#33181=CARTESIAN_POINT ( 'NONE',  ( -110.5228709571500332, -24.63345952396256422, 9.038047939301501188 ) ) ;
#33184=ORIENTED_EDGE ( 'NONE', *, *, #19191, .F. ) ;
#33186=B_SPLINE_CURVE_WITH_KNOTS ( 'NONE', 3,
 ( #78529, #30872, #55730, #46610 ),
 .UNSPECIFIED., .F., .F.,
 ( 4, 4 ),
 ( 0.000000000000000000, 1.000000000000000000 ),
 .UNSPECIFIED. ) ;
#33187=CARTESIAN_POINT ( 'NONE',  ( -100.6228709571501128, -24.14321612903118464, -0.2833117244521107247 ) ) ;
#33188=CARTESIAN_POINT ( 'NONE',  ( -19.87929632332335927, 2.386914507623989490, -1.500000000000002220 ) ) ;
#33190=CARTESIAN_POINT ( 'NONE',  ( -16.09219062524700661, 13.46031615953476468, 11.49999999999999645 ) ) ;
#33192=CARTESIAN_POINT ( 'NONE',  ( -70.62368314357276233, -25.00182538069146787, 7.747789668545044250 ) ) ;
#33193=CARTESIAN_POINT ( 'NONE',  ( -0.5447568859041533873, -22.05808898580190558, -1.500000000000002220 ) ) ;
#33194=AXIS2_PLACEMENT_3D ( 'NONE', #80228, #57415, #65534 ) ;
#33195=CARTESIAN_POINT ( 'NONE',  ( -59.52287095715009002, -23.47593901973090524, -1.443836447538997092 ) ) ;
#33196=ORIENTED_EDGE ( 'NONE', *, *, #100143, .F. ) ;
#33197=PLANE ( 'NONE',  #20841 ) ;
#33199=CARTESIAN_POINT ( 'NONE',  ( -72.52211250399544440, -23.48783264082477018, -1.443836473390095021 ) ) ;
#33200=ORIENTED_EDGE ( 'NONE', *, *, #19968, .T. ) ;
#33201=CARTESIAN_POINT ( 'NONE',  ( -92.62287095715005592, -23.47596703998600631, 11.44779298504227860 ) ) ;
#33202=ORIENTED_EDGE ( 'NONE', *, *, #2856, .F. ) ;
#33203=ORIENTED_EDGE ( 'NONE', *, *, #13158, .T. ) ;
#33204=CARTESIAN_POINT ( 'NONE',  ( -79.52287095715010423, -23.47593901973090524, -1.443836447538996870 ) ) ;
#33205=LINE ( 'NONE', #1765, #22713 ) ;
#33207=CARTESIAN_POINT ( 'NONE',  ( -11.60840874443078263, -16.91462557209307960, -1.500000000000002220 ) ) ;
#33210=VERTEX_POINT ( 'NONE', #80099 ) ;
#33211=CARTESIAN_POINT ( 'NONE',  ( -99.63518257809350587, -25.29661202606573411, 5.472634000556907630 ) ) ;
#33214=CARTESIAN_POINT ( 'NONE',  ( -18.01732314745861530, 13.19606014829601826, -1.500000000000002220 ) ) ;
#33215=CARTESIAN_POINT ( 'NONE',  ( -111.6228709571500559, -24.64965695001468404, 8.947790433994176951 ) ) ;
#33216=DIRECTION ( 'NONE',  ( 1.000000000000000000, 3.773278334444166432E-23, 8.201307841325785021E-29 ) ) ;
#33217=VERTEX_POINT ( 'NONE', #10089 ) ;
#33218=CARTESIAN_POINT ( 'NONE',  ( -101.6228709571500559, -23.48783264082479505, -1.443836473390062380 ) ) ;
#33220=CARTESIAN_POINT ( 'NONE',  ( -13.77211689728001964, -15.67653869864640903, -1.500000000000002220 ) ) ;
#33223=ORIENTED_EDGE ( 'NONE', *, *, #61418, .T. ) ;
#33225=CARTESIAN_POINT ( 'NONE',  ( -70.28247728326880406, -25.03149372358761227, 7.560917013690431787 ) ) ;
#33226=CARTESIAN_POINT ( 'NONE',  ( 5.245434476726341444, -20.39595507048906242, -1.500000000000002220 ) ) ;
#33227=ADVANCED_FACE ( 'NONE', ( #42058 ), #41047, .T. ) ;
#33229=CARTESIAN_POINT ( 'NONE',  ( -85.62287095715004170, -23.48783264082478794, -1.443836473390063713 ) ) ;
#33231=CARTESIAN_POINT ( 'NONE',  ( -120.5163168400560352, -25.00182538069147142, 7.747789668545046027 ) ) ;
#33232=CARTESIAN_POINT ( 'NONE',  ( -86.51786200934954252, -23.73791477778911840, 11.05961554403170766 ) ) ;
#33233=PLANE ( 'NONE',  #83779 ) ;
#33234=CARTESIAN_POINT ( 'NONE',  ( -18.45943378446990835, 11.37049804852326140, -1.500000000000002220 ) ) ;
#33236=CARTESIAN_POINT ( 'NONE',  ( -12.31279356157217109, -18.55646752483835016, 11.49999999999999645 ) ) ;
#33237=ORIENTED_EDGE ( 'NONE', *, *, #65059, .F. ) ;
#33238=CARTESIAN_POINT ( 'NONE',  ( -51.52657066994672164, -25.31441930330192491, 6.155056426832686611 ) ) ;
#33241=ORIENTED_EDGE ( 'NONE', *, *, #54991, .T. ) ;
#33243=VERTEX_POINT ( 'NONE', #43914 ) ;
#33248=CARTESIAN_POINT ( 'NONE',  ( 9.931738293602487389, -17.53800358597336384, -1.500000000000002220 ) ) ;
#33249=CARTESIAN_POINT ( 'NONE',  ( -126.5228709571500332, -24.50321055353804311, 9.387540953477511607 ) ) ;
#33251=CARTESIAN_POINT ( 'NONE',  ( -130.5728709571500872, -24.96453677868172605, 8.261112634458179116 ) ) ;
#33252=CARTESIAN_POINT ( 'NONE',  ( -22.05133119090760019, 4.102169094691678453, -1.500000000000002220 ) ) ;
#33253=EDGE_LOOP ( 'NONE', ( #13593, #39141, #92755, #60300 ) ) ;
#33254=ORIENTED_EDGE ( 'NONE', *, *, #98023, .T. ) ;
#33255=CARTESIAN_POINT ( 'NONE',  ( -34.52287095715006160, -24.64965694238575011, 8.947790433994207149 ) ) ;
#33256=CARTESIAN_POINT ( 'NONE',  ( -101.5487862718491670, -24.51419770103158413, 9.386484678747175181 ) ) ;
#33257=CARTESIAN_POINT ( 'NONE',  ( -110.5562042904833930, -25.00182538069145721, 7.747789668545099317 ) ) ;
#33258=CARTESIAN_POINT ( 'NONE',  ( -48.92287095715006728, -23.47593901973090169, -1.443836447538997758 ) ) ;
#33259=CARTESIAN_POINT ( 'NONE',  ( -63.91063458982754497, -25.14064729901805606, 2.712351064733618422 ) ) ;
#33260=CARTESIAN_POINT ( 'NONE',  ( -18.73025074496528219, 5.678645368852136777, -1.500000000000002220 ) ) ;
#33262=ORIENTED_EDGE ( 'NONE', *, *, #26993, .T. ) ;
#33263=CARTESIAN_POINT ( 'NONE',  ( 16.66814584454133907, -13.58961022886752978, -1.500000000000002220 ) ) ;
#33264=FACE_OUTER_BOUND ( 'NONE', #85202, .T. ) ;
#33265=CARTESIAN_POINT ( 'NONE',  ( -38.58953762381672448, -23.47593901973091235, -1.443836447539011525 ) ) ;
#33268=CARTESIAN_POINT ( 'NONE',  ( 6.461317529299694051, 22.01590093704556850, -1.500000000000002220 ) ) ;
#33272=CARTESIAN_POINT ( 'NONE',  ( -70.60159577184752777, -25.31102706251628831, 5.335685664145170648 ) ) ;
#33273=CARTESIAN_POINT ( 'NONE',  ( -19.48533387766964964, -5.011242947278518045, 11.49999999999999645 ) ) ;
#33274=CARTESIAN_POINT ( 'NONE',  ( -68.55620429048340725, -23.47596703998600276, 11.44779298504227505 ) ) ;
#33275=CARTESIAN_POINT ( 'NONE',  ( -32.52609515912349281, -24.66019654487198665, 8.947790411086131712 ) ) ;
#33278=CARTESIAN_POINT ( 'NONE',  ( -40.62287095715004170, -24.99132157543083466, 2.256160258750667502 ) ) ;
#33279=CARTESIAN_POINT ( 'NONE',  ( 19.67252036444665109, 2.607452956813616218, -1.500000000000002220 ) ) ;
#33281=CARTESIAN_POINT ( 'NONE',  ( 14.19269941865516671, -13.59168563846684563, -1.500000000000002220 ) ) ;
#33283=CARTESIAN_POINT ( 'NONE',  ( -42.64094106932928696, -24.15543982623907127, -0.2315651400026575435 ) ) ;
#33284=B_SPLINE_CURVE_WITH_KNOTS ( 'NONE', 3,
 ( #82498, #12981, #52062, #47440 ),
 .UNSPECIFIED., .F., .F.,
 ( 4, 4 ),
 ( 0.5809148170514456533, 0.5899212483235611870 ),
 .UNSPECIFIED. ) ;
#33285=CARTESIAN_POINT ( 'NONE',  ( -32.52287095715005449, -23.72747288104469732, -1.053458166803228346 ) ) ;
#33288=CARTESIAN_POINT ( 'NONE',  ( -39.04303308397305727, -25.28006866179717349, 4.215216948383927686 ) ) ;
#33289=CARTESIAN_POINT ( 'NONE',  ( 16.39479758508079144, -12.47777281027006424, 11.49999999999999645 ) ) ;
#33291=EDGE_CURVE ( 'NONE', #4166, #13524, #50162, .T. ) ;
#33292=CARTESIAN_POINT ( 'NONE',  ( -33.62287095715005592, -23.47596703998600276, 11.44779298504227505 ) ) ;
#33293=CARTESIAN_POINT ( 'NONE',  ( -18.09186581907994196, -13.49991075323410250, 11.49999999999999645 ) ) ;
#33295=CARTESIAN_POINT ( 'NONE',  ( -69.41396772704672458, -25.25639482192426044, 6.552775495269651529 ) ) ;
#33296=CARTESIAN_POINT ( 'NONE',  ( -123.6228709571500559, -29.50248528299804818, 1.056150453629045360 ) ) ;
#33297=CARTESIAN_POINT ( 'NONE',  ( -97.63537331154846299, -23.73766607897670156, -1.055555164236452237 ) ) ;
#33298=CARTESIAN_POINT ( 'NONE',  ( -64.52287095715006160, -23.48783264082476308, -1.443836473390094355 ) ) ;
#33300=CARTESIAN_POINT ( 'NONE',  ( -110.6228709571500701, -24.82576562982393042, 8.398263435472971494 ) ) ;
#33303=CARTESIAN_POINT ( 'NONE',  ( -80.39192082756260049, -25.31596222338272639, 4.967919814078590512 ) ) ;
#33304=CARTESIAN_POINT ( 'NONE',  ( -7.631545101075025705, 21.52643039700453897, 11.49999999999998934 ) ) ;
#33305=CARTESIAN_POINT ( 'NONE',  ( -111.2429372202815472, -25.24710330342993458, 3.804655253729887665 ) ) ;
#33306=CARTESIAN_POINT ( 'NONE',  ( -115.5228709571500190, -24.82576562948886689, 8.398263436605494903 ) ) ;
#33307=CARTESIAN_POINT ( 'NONE',  ( -82.50963591457735902, -24.15620529776628089, 10.23563542870660825 ) ) ;
#33309=CARTESIAN_POINT ( 'NONE',  ( -9.984083066403742990, 20.14924292131567185, 11.49999999999999645 ) ) ;
#33310=EDGE_LOOP ( 'NONE', ( #20032, #85998, #25083, #96983 ) ) ;
#33311=DIRECTION ( 'NONE',  ( -3.773278334453079618E-23, 0.9999999999976377785, 2.173523156925979975E-06 ) ) ;
#33312=CARTESIAN_POINT ( 'NONE',  ( -21.51515180086577317, 4.489188270810763548, -1.500000000000002220 ) ) ;
#33313=CARTESIAN_POINT ( 'NONE',  ( -41.52287095715006870, -29.50248528299804818, 1.056150453629031594 ) ) ;
#33314=CARTESIAN_POINT ( 'NONE',  ( -34.60129046058678881, -23.96169478059712077, 10.65365249895718769 ) ) ;
#33315=CARTESIAN_POINT ( 'NONE',  ( -68.93918693012690824, -25.24795196732124936, 6.184868460502651821 ) ) ;
#33317=CARTESIAN_POINT ( 'NONE',  ( -92.58953762381672448, -24.64898659630368627, 1.056161002820388717 ) ) ;
#33319=ORIENTED_EDGE ( 'NONE', *, *, #46272, .F. ) ;
#33320=CARTESIAN_POINT ( 'NONE',  ( -19.72667040167412722, -5.651925516699977337, -1.500000000000002220 ) ) ;
#33322=ORIENTED_EDGE ( 'NONE', *, *, #82647, .F. ) ;
#33324=VERTEX_POINT ( 'NONE', #74844 ) ;
#33325=CARTESIAN_POINT ( 'NONE',  ( -80.48900664166535535, -25.13313949306887807, 7.101635536975466678 ) ) ;
#33326=CARTESIAN_POINT ( 'NONE',  ( 3.535601659403828201, -22.84449096179584160, 11.49999999999998934 ) ) ;
#33328=CARTESIAN_POINT ( 'NONE',  ( -18.82647582233506611, 7.659846263794035437, -1.500000000000002220 ) ) ;
#33329=ORIENTED_EDGE ( 'NONE', *, *, #9701, .T. ) ;
#33331=CARTESIAN_POINT ( 'NONE',  ( -29.58011630254760860, -24.43483877924948544, 9.386484716961753350 ) ) ;
#33332=ADVANCED_FACE ( 'NONE', ( #48163 ), #19119, .T. ) ;
#33333=FACE_OUTER_BOUND ( 'NONE', #99625, .T. ) ;
#33334=CARTESIAN_POINT ( 'NONE',  ( -63.52287095715010423, -24.33927499327854349, 9.819080762295818943 ) ) ;
#33335=CARTESIAN_POINT ( 'NONE',  ( -21.45671390985790694, -1.711987587955616119, 11.49999999999999645 ) ) ;
#33336=ORIENTED_EDGE ( 'NONE', *, *, #26865, .F. ) ;
#33337=CARTESIAN_POINT ( 'NONE',  ( -28.10168127693285101, -25.21531671887374060, 2.337526732200711166 ) ) ;
#33338=DIRECTION ( 'NONE',  ( 0.000000000000000000, -2.173523156925980399E-06, 0.9999999999976378895 ) ) ;
#33339=VERTEX_POINT ( 'NONE', #67262 ) ;
#33340=CARTESIAN_POINT ( 'NONE',  ( -20.46667790307254009, -3.548193229090686796, 11.49999999999998934 ) ) ;
#33341=ORIENTED_EDGE ( 'NONE', *, *, #64617, .T. ) ;
#33342=EDGE_CURVE ( 'NONE', #98743, #49833, #95315, .T. ) ;
#33343=CARTESIAN_POINT ( 'NONE',  ( -125.5202182622694949, -24.52300882791529801, 0.6510814631126508045 ) ) ;
#33346=CARTESIAN_POINT ( 'NONE',  ( -77.52287095715006160, -24.64898659630367916, 1.056161002820826145 ) ) ;
#33347=CARTESIAN_POINT ( 'NONE',  ( -97.52287095715004739, -23.73934037231758154, 11.05740245334328797 ) ) ;
#33349=VERTEX_POINT ( 'NONE', #52523 ) ;
#33351=DIRECTION ( 'NONE',  ( -0.8899332505568755547, 9.913238957044378156E-07, -0.4560907909093217527 ) ) ;
#33352=CARTESIAN_POINT ( 'NONE',  ( -68.62287095715002749, -23.73934037231756378, 11.05740245334329153 ) ) ;
#33354=CARTESIAN_POINT ( 'NONE',  ( -78.52287095715004739, -24.50216790748204332, 0.6166512839542561686 ) ) ;
#33355=CARTESIAN_POINT ( 'NONE',  ( 7.855769811932122870, -20.56199346058834720, 11.49999999999999645 ) ) ;
#33358=CARTESIAN_POINT ( 'NONE',  ( -103.5492918164049598, -24.51314013834316086, 0.6176544820404170633 ) ) ;
#33359=CARTESIAN_POINT ( 'NONE',  ( -16.99934442671578694, -14.85117937636706031, 11.49999999999998934 ) ) ;
#33362=ORIENTED_EDGE ( 'NONE', *, *, #45186, .F. ) ;
#33364=B_SPLINE_CURVE_WITH_KNOTS ( 'NONE', 3,
 ( #82354, #49938, #51419, #10857 ),
 .UNSPECIFIED., .F., .F.,
 ( 4, 4 ),
 ( 0.2406718578826401722, 0.2496782891547557337 ),
 .UNSPECIFIED. ) ;
#33365=CARTESIAN_POINT ( 'NONE',  ( -79.52287095715006160, -29.50248528299804818, 1.056150453629038477 ) ) ;
#33367=CARTESIAN_POINT ( 'NONE',  ( -57.49288415400445018, -24.51419770103157703, 9.386484678747175181 ) ) ;
#33369=CARTESIAN_POINT ( 'NONE',  ( -6.524719417830534773, 20.15472526627327454, 11.49999999999998934 ) ) ;
#33370=CARTESIAN_POINT ( 'NONE',  ( -82.62287095715005592, -23.48783264082478084, -1.443836473390065933 ) ) ;
#33371=CARTESIAN_POINT ( 'NONE',  ( -92.62287095715005592, -24.65952944569304606, 1.056160979905700348 ) ) ;
#33372=DIRECTION ( 'NONE',  ( -3.773278334453079618E-23, 0.9999999999976377785, 2.173523156925979975E-06 ) ) ;
#33373=CARTESIAN_POINT ( 'NONE',  ( -26.09636659181000695, -29.50249372523856195, 4.940277699495910113 ) ) ;
#33374=CARTESIAN_POINT ( 'NONE',  ( -11.95080204275630464, 18.75100984808165094, -1.500000000000002220 ) ) ;
#33375=CARTESIAN_POINT ( 'NONE',  ( -114.5530387260713638, -24.34968618360934300, 0.1864209137778971848 ) ) ;
#33376=ORIENTED_EDGE ( 'NONE', *, *, #76585, .T. ) ;
#33378=CARTESIAN_POINT ( 'NONE',  ( -30.57287095715006231, -23.47594215783195537, -5.102550391006585557E-05 ) ) ;
#33379=CARTESIAN_POINT ( 'NONE',  ( -19.08929872761019908, -3.557156390981079053, 11.49999999999999645 ) ) ;
#33380=ADVANCED_FACE ( 'NONE', ( #92563 ), #84954, .F. ) ;
#33381=B_SPLINE_CURVE_WITH_KNOTS ( 'NONE', 3,
 ( #74515, #50689, #35468, #36452, #88252, #20219 ),
 .UNSPECIFIED., .F., .F.,
 ( 4, 2, 4 ),
 ( 0.000000000000000000, 0.001380901958385379220, 0.002761803916770758441 ),
 .UNSPECIFIED. ) ;
#33384=CARTESIAN_POINT ( 'NONE',  ( 15.68791110202092476, 11.56419973807686219, 11.49999999999998934 ) ) ;
#33385=CARTESIAN_POINT ( 'NONE',  ( 16.75108703964928480, -13.32659110743468212, -1.500000000000002220 ) ) ;
#33387=CARTESIAN_POINT ( 'NONE',  ( -60.62371847853048479, -25.00182538069856619, 7.747789668514392325 ) ) ;
#33388=DIRECTION ( 'NONE',  ( -2.006501617224642956E-17, 0.5416355246053408123, -0.8406134417706495610 ) ) ;
#33389=CARTESIAN_POINT ( 'NONE',  ( -59.62287095715004881, -29.50250786944525672, 11.44777988621623876 ) ) ;
#33390=CARTESIAN_POINT ( 'NONE',  ( 18.51665531608540860, 13.21585733361752801, -1.500000000000002220 ) ) ;
#33392=CARTESIAN_POINT ( 'NONE',  ( -102.5109985006918976, -24.51314013834317151, 0.6176544820404245018 ) ) ;
#33394=CARTESIAN_POINT ( 'NONE',  ( 9.006517291608927778, -17.75031788249398446, 11.49999999999999645 ) ) ;
#33396=ADVANCED_FACE ( 'NONE', ( #5348 ), #82955, .T. ) ;
#33399=ADVANCED_FACE ( 'NONE', ( #22540 ), #44421, .F. ) ;
#33400=VERTEX_POINT ( 'NONE', #45912 ) ;
#33401=CARTESIAN_POINT ( 'NONE',  ( -50.06403713569625324, -25.12896391188073508, 7.067345851436766857 ) ) ;
#33402=CARTESIAN_POINT ( 'NONE',  ( -32.40341606139129738, -25.31600595412499644, 6.101236642668423471 ) ) ;
#33404=CARTESIAN_POINT ( 'NONE',  ( -15.38093110518717666, 15.28219592669002402, 11.49999999999998934 ) ) ;
#33406=CARTESIAN_POINT ( 'NONE',  ( -17.86923650574433609, -7.721772263035739492, -1.500000000000002220 ) ) ;
#33408=CARTESIAN_POINT ( 'NONE',  ( -93.52287095715009002, -23.48783264082477018, -1.443836473390088360 ) ) ;
#33410=CARTESIAN_POINT ( 'NONE',  ( -20.15914900662387055, -2.930279687489938389, 11.49999999999999645 ) ) ;
#33412=EDGE_CURVE ( 'NONE', #75504, #54444, #80752, .T. ) ;
#33417=CARTESIAN_POINT ( 'NONE',  ( -79.45125215927727425, -25.10767898202385950, 7.188516721831696543 ) ) ;
#33421=CARTESIAN_POINT ( 'NONE',  ( -70.52287095715007581, -29.50249982740957577, 7.747779886224967605 ) ) ;
#33424=ADVANCED_FACE ( 'NONE', ( #92070 ), #73424, .T. ) ;
#33427=ORIENTED_EDGE ( 'NONE', *, *, #53351, .T. ) ;
#33430=EDGE_CURVE ( 'NONE', #49698, #38599, #16947, .T. ) ;
#33431=CARTESIAN_POINT ( 'NONE',  ( -10.62949710387652758, 20.32685691788189075, 11.49999999999999645 ) ) ;
#33432=CARTESIAN_POINT ( 'NONE',  ( 15.23092229589061830, -16.91372389758942418, -1.500000000000002220 ) ) ;
#33435=CARTESIAN_POINT ( 'NONE',  ( -90.55814957459756442, -23.85016227208580730, -0.8807180028928305315 ) ) ;
#33436=CARTESIAN_POINT ( 'NONE',  ( -82.55620429048340725, -23.48783264082478084, -1.443836473390066377 ) ) ;
#33437=CARTESIAN_POINT ( 'NONE',  ( -17.40403014803320758, -13.24600170205644289, -1.500000000000002220 ) ) ;
#33438=DIRECTION ( 'NONE',  ( -1.000000000000000000, -3.773278334444167608E-23, -8.201307833595939069E-29 ) ) ;
#33440=CARTESIAN_POINT ( 'NONE',  ( -122.5190359270850990, -24.51314013834316086, 0.6176544820404212821 ) ) ;
#33441=CARTESIAN_POINT ( 'NONE',  ( -81.55620429048342146, -23.47593901973091235, -1.443836447539004642 ) ) ;
#33442=VERTEX_POINT ( 'NONE', #63141 ) ;
#33443=CARTESIAN_POINT ( 'NONE',  ( 8.094744887094867281, -18.73235182305680624, 11.49999999999998934 ) ) ;
#33444=ORIENTED_EDGE ( 'NONE', *, *, #11053, .F. ) ;
#33446=CARTESIAN_POINT ( 'NONE',  ( -4.971178678486217528, -22.47594730032828281, -1.500000000000002220 ) ) ;
#33450=LINE ( 'NONE', #64439, #41262 ) ;
#33451=CARTESIAN_POINT ( 'NONE',  ( -42.52287095715005449, -23.47593901973090169, -1.443836447538997092 ) ) ;
#33453=CARTESIAN_POINT ( 'NONE',  ( -116.6623051836383667, -25.28353586862649038, 5.756525109479947666 ) ) ;
#33454=CARTESIAN_POINT ( 'NONE',  ( 14.87313431965483801, 15.23822737908125902, 11.49999999999999645 ) ) ;
#33455=ORIENTED_EDGE ( 'NONE', *, *, #68209, .T. ) ;
#33457=CARTESIAN_POINT ( 'NONE',  ( -15.91109736606077441, 15.52988587838853540, 11.49999999999998934 ) ) ;
#33458=CARTESIAN_POINT ( 'NONE',  ( 20.52162115075873672, 2.272738508513782119, -1.500000000000002220 ) ) ;
#33461=EDGE_CURVE ( 'NONE', #11978, #82726, #91516, .T. ) ;
#33463=CARTESIAN_POINT ( 'NONE',  ( -69.85793399335128129, -25.20650855361216713, 6.812664954086296909 ) ) ;
#33464=VERTEX_POINT ( 'NONE', #87462 ) ;
#33465=FACE_OUTER_BOUND ( 'NONE', #8749, .T. ) ;
#33467=CARTESIAN_POINT ( 'NONE',  ( -58.50878158211892810, -23.96169478059713143, 10.65365249895718058 ) ) ;
#33468=DIRECTION ( 'NONE',  ( 0.000000000000000000, 2.173523156925980399E-06, -0.9999999999976378895 ) ) ;
#33469=CARTESIAN_POINT ( 'NONE',  ( -13.97254113366623152, 15.51630364309664856, -1.500000000000002220 ) ) ;
#33470=CARTESIAN_POINT ( 'NONE',  ( -15.04333773895388937, -15.80532200100455498, 11.49999999999999645 ) ) ;
#33472=LINE ( 'NONE', #64463, #88837 ) ;
#33473=CARTESIAN_POINT ( 'NONE',  ( 22.09666729679958053, 4.251135690456572469, 11.49999999999998934 ) ) ;
#33475=CARTESIAN_POINT ( 'NONE',  ( -5.518977837361389582, -20.17201009624758257, -1.500000000000002220 ) ) ;
#33476=B_SPLINE_CURVE_WITH_KNOTS ( 'NONE', 3,
 ( #84818, #15303, #8209, #16311 ),
 .UNSPECIFIED., .F., .F.,
 ( 4, 4 ),
 ( 0.000000000000000000, 9.999999999998897304E-05 ),
 .UNSPECIFIED. ) ;
#33477=FACE_OUTER_BOUND ( 'NONE', #82413, .T. ) ;
#33478=B_SPLINE_CURVE_WITH_KNOTS ( 'NONE', 3,
 ( #28394, #14670, #69961, #29898, #68963, #99887 ),
 .UNSPECIFIED., .F., .F.,
 ( 4, 2, 4 ),
 ( 1.570887131794333942E-05, 0.001396322306279758904, 0.002776935741241574537 ),
 .UNSPECIFIED. ) ;
#33479=CARTESIAN_POINT ( 'NONE',  ( -52.55620429048339304, -24.66019654487199020, 8.947790411086135265 ) ) ;
#33480=CARTESIAN_POINT ( 'NONE',  ( -68.58953762381672448, -23.47593901973091235, -1.443836447539006196 ) ) ;
#33481=VERTEX_POINT ( 'NONE', #71747 ) ;
#33484=CARTESIAN_POINT ( 'NONE',  ( -52.50176957019452573, -24.15543982623907482, -0.2315651400026529916 ) ) ;
#33487=ADVANCED_FACE ( 'NONE', ( #24051 ), #55527, .T. ) ;
#33488=CARTESIAN_POINT ( 'NONE',  ( -1.242826169824672977, 21.35102975155811222, -1.500000000000002220 ) ) ;
#33489=CARTESIAN_POINT ( 'NONE',  ( 21.44611857939883137, 6.294191480875499067, 11.49999999999999645 ) ) ;
#33491=CARTESIAN_POINT ( 'NONE',  ( -59.52287095715007581, -23.96127896941631974, -0.6493128931038036900 ) ) ;
#33493=CARTESIAN_POINT ( 'NONE',  ( 9.758084087097168791, -18.66043984184860349, -1.500000000000002220 ) ) ;
#33494=CARTESIAN_POINT ( 'NONE',  ( -30.64649332944061655, -23.48782090502276176, 11.44779287168131710 ) ) ;
#33495=CARTESIAN_POINT ( 'NONE',  ( 1.402406813841059030, 19.88454085074057076, -1.500000000000002220 ) ) ;
#33498=CARTESIAN_POINT ( 'NONE',  ( -113.5228709571500758, -23.48783264082477373, -1.443836473390082586 ) ) ;
#33499=CARTESIAN_POINT ( 'NONE',  ( -6.199593828526920092, 21.14725108817225419, -1.500000000000002220 ) ) ;
#33500=ORIENTED_EDGE ( 'NONE', *, *, #3628, .F. ) ;
#33501=CARTESIAN_POINT ( 'NONE',  ( -65.48791648632810336, -24.83644354573578994, 8.397322867130098345 ) ) ;
#33504=CARTESIAN_POINT ( 'NONE',  ( -40.63161819696095733, -25.27956070701981162, 5.540357918835671747 ) ) ;
#33505=ADVANCED_FACE ( 'NONE', ( #15937 ), #78827, .F. ) ;
#33506=VECTOR ( 'NONE', #85709, 1000.000000000000114 ) ;
#33507=EDGE_CURVE ( 'NONE', #87407, #34175, #83061, .T. ) ;
#33508=CARTESIAN_POINT ( 'NONE',  ( -62.50437674283933376, -24.15620529776627734, 10.23563542870660825 ) ) ;
#33510=EDGE_CURVE ( 'NONE', #78003, #76683, #98693, .T. ) ;
#33511=CARTESIAN_POINT ( 'NONE',  ( -61.62287095715004881, -24.65952944569304606, 1.056160979905695907 ) ) ;
#33512=CARTESIAN_POINT ( 'NONE',  ( -1.825377252022436281, -21.23478267787193730, 11.49999999999998934 ) ) ;
#33513=CARTESIAN_POINT ( 'NONE',  ( -121.5895376238167103, -24.64965694238408034, 8.947790433994647685 ) ) ;
#33514=CARTESIAN_POINT ( 'NONE',  ( -117.5228709571500758, -23.48786465467241769, 11.44779295918253759 ) ) ;
#33517=CARTESIAN_POINT ( 'NONE',  ( -12.77507031947300042, 18.62636059118606724, -1.500000000000002220 ) ) ;
#33519=ORIENTED_EDGE ( 'NONE', *, *, #6598, .F. ) ;
#33521=CARTESIAN_POINT ( 'NONE',  ( -31.50372651583977657, -23.96169478059712432, 10.65365249895719124 ) ) ;
#33522=CARTESIAN_POINT ( 'NONE',  ( -2.355416116969162754, -19.56741566493107598, 11.49999999999999645 ) ) ;
#33523=CARTESIAN_POINT ( 'NONE',  ( -41.22287095715007155, -23.47593901973090169, -1.443836447538997980 ) ) ;
#33524=B_SPLINE_CURVE_WITH_KNOTS ( 'NONE', 3,
 ( #10698, #34037, #41660, #65013 ),
 .UNSPECIFIED., .F., .F.,
 ( 4, 4 ),
 ( 0.6002145229766536749, 0.6092209542487688756 ),
 .UNSPECIFIED. ) ;
#33525=DIRECTION ( 'NONE',  ( -3.773278334453079618E-23, 0.9999999999976377785, 2.173523156925979975E-06 ) ) ;
#33526=EDGE_CURVE ( 'NONE', #51543, #36438, #18913, .T. ) ;
#33527=ORIENTED_EDGE ( 'NONE', *, *, #4819, .F. ) ;
#33530=CARTESIAN_POINT ( 'NONE',  ( -124.6256213753410691, -23.73791477778912551, 11.05961554403169878 ) ) ;
#33531=AXIS2_PLACEMENT_3D ( 'NONE', #39954, #17111, #9001 ) ;
#33535=CARTESIAN_POINT ( 'NONE',  ( -19.30086548479123465, -4.275078920326023990, 11.49999999999998934 ) ) ;
#33538=CARTESIAN_POINT ( 'NONE',  ( -18.67835518149133378, -7.740158416121700746, 11.49999999999999645 ) ) ;
#33540=EDGE_CURVE ( 'NONE', #55957, #8604, #89009, .T. ) ;
#33542=ORIENTED_EDGE ( 'NONE', *, *, #64893, .F. ) ;
#33544=CARTESIAN_POINT ( 'NONE',  ( -81.26450725226473537, -25.30500210224441560, 5.136533544873633339 ) ) ;
#33545=CARTESIAN_POINT ( 'NONE',  ( -77.52287095715006160, -24.64965694238575011, 8.947790433994198267 ) ) ;
#33546=CARTESIAN_POINT ( 'NONE',  ( -112.6228709571500559, -24.64965695001469115, 8.947790433994176951 ) ) ;
#33547=CARTESIAN_POINT ( 'NONE',  ( -39.62287095715005592, -24.65952944569304606, 1.056160979905692354 ) ) ;
#33549=CARTESIAN_POINT ( 'NONE',  ( -18.22994410263883225, 8.285605901428201747, 11.49999999999998934 ) ) ;
#33550=EDGE_CURVE ( 'NONE', #63463, #7016, #76949, .T. ) ;
#33551=CARTESIAN_POINT ( 'NONE',  ( -99.12594121859551421, -25.10935281042543821, 3.952133049703926648 ) ) ;
#33552=ORIENTED_EDGE ( 'NONE', *, *, #73971, .T. ) ;
#33558=CARTESIAN_POINT ( 'NONE',  ( -100.6228709571500559, -24.99156045073393173, 7.747789690856161648 ) ) ;
#33559=B_SPLINE_CURVE_WITH_KNOTS ( 'NONE', 3,
 ( #81562, #4443, #82054, #12037, #28264, #34885 ),
 .UNSPECIFIED., .F., .F.,
 ( 4, 2, 4 ),
 ( 0.000000000000000000, 0.001380764517853248600, 0.002761529035706497201 ),
 .UNSPECIFIED. ) ;
#33560=CARTESIAN_POINT ( 'NONE',  ( -84.52287095715006160, -29.50248528299804818, 1.056150453629038477 ) ) ;
#33561=CARTESIAN_POINT ( 'NONE',  ( -101.5413594152072960, -25.20011968295217386, 3.398381376179529401 ) ) ;
#33565=CARTESIAN_POINT ( 'NONE',  ( -49.51564274782410280, -25.25375110409948576, 3.879908378599426833 ) ) ;
#33566=VECTOR ( 'NONE', #40356, 1000.000000000000114 ) ;
#33567=ORIENTED_EDGE ( 'NONE', *, *, #79220, .T. ) ;
#33568=AXIS2_PLACEMENT_3D ( 'NONE', #38491, #23751, #52720 ) ;
#33569=CARTESIAN_POINT ( 'NONE',  ( 5.353267490507026771, -19.58905154090721368, 11.49999999999998934 ) ) ;
#33570=EDGE_LOOP ( 'NONE', ( #69007, #6534, #88284, #93722 ) ) ;
#33572=CARTESIAN_POINT ( 'NONE',  ( -127.5214690509877187, -24.15620529776629155, 10.23563542870658694 ) ) ;
#33573=ORIENTED_EDGE ( 'NONE', *, *, #69772, .T. ) ;
#33574=DIRECTION ( 'NONE',  ( -0.000000000000000000, 2.173523156925979552E-06, -0.9999999999976378895 ) ) ;
#33575=CARTESIAN_POINT ( 'NONE',  ( -50.28030459868799795, -25.26264177999245319, 7.099251632680519286 ) ) ;
#33576=CARTESIAN_POINT ( 'NONE',  ( -30.47287095715006089, -24.48470683598323916, 9.426283873570685756 ) ) ;
#33577=CARTESIAN_POINT ( 'NONE',  ( 14.48694714638828884, 15.39972936300609341, 11.49999999999999645 ) ) ;
#33578=CARTESIAN_POINT ( 'NONE',  ( 20.51613352552997327, 8.347415244503286758, -1.500000000000002220 ) ) ;
#33579=CARTESIAN_POINT ( 'NONE',  ( 18.12345787009687115, -9.690629616749632191, -1.500000000000002220 ) ) ;
#33580=ORIENTED_EDGE ( 'NONE', *, *, #92724, .F. ) ;
#33581=CARTESIAN_POINT ( 'NONE',  ( -94.52287095715003318, -24.66019654487199730, 8.947790411086124607 ) ) ;
#33582=EDGE_LOOP ( 'NONE', ( #12254, #92608, #83579, #74133 ) ) ;
#33583=PLANE ( 'NONE',  #15528 ) ;
#33584=CARTESIAN_POINT ( 'NONE',  ( -80.62287095715005592, -23.47593901973091235, -1.443836447539004642 ) ) ;
#33585=VERTEX_POINT ( 'NONE', #89958 ) ;
#33587=VERTEX_POINT ( 'NONE', #27069 ) ;
#33588=DIRECTION ( 'NONE',  ( 0.000000000000000000, -2.173523156925979552E-06, 0.9999999999976378895 ) ) ;
#33589=CARTESIAN_POINT ( 'NONE',  ( -127.6228709571500275, -23.73934037231758154, 11.05740245334327732 ) ) ;
#33591=CARTESIAN_POINT ( 'NONE',  ( 18.27903665858761073, 9.701928907310005457, -1.500000000000002220 ) ) ;
#33592=CARTESIAN_POINT ( 'NONE',  ( -14.64807036877012258, -15.96857234361563904, 11.49999999999999645 ) ) ;
#33594=CARTESIAN_POINT ( 'NONE',  ( -98.98242597041321744, -25.29000073409625315, 5.621580901835582011 ) ) ;
#33596=CARTESIAN_POINT ( 'NONE',  ( -111.7342643247342551, -25.26010494679146490, 3.947561888149926368 ) ) ;
#33597=CARTESIAN_POINT ( 'NONE',  ( 14.42577177192597482, -17.14957960503723911, -1.500000000000002220 ) ) ;
#33598=LINE ( 'NONE', #50830, #20549 ) ;
#33603=B_SPLINE_SURFACE_WITH_KNOTS ( 'NONE', 3, 3, ( 
 ( #12375, #74286, #91995, #91492 ),
 ( #99099, #76752, #14366, #21971 ),
 ( #67687, #83383, #21473, #38708 ),
 ( #6264, #76264, #84882, #100083 ),
 ( #36723, #77259, #52953, #92493 ),
 ( #69163, #60575, #82883, #90999 ),
 ( #13369, #30597, #7253, #75765 ) ),
 .UNSPECIFIED., .F., .F., .F.,
 ( 4, 3, 4 ),
 ( 4, 4 ),
 ( 0.0004766839783842195507, 0.1029713700210906219, 0.2054660560637970312 ),
 ( 0.4396058254596823534, 0.4408213833358379796 ),
 .UNSPECIFIED. ) ;
#33606=ORIENTED_EDGE ( 'NONE', *, *, #19791, .T. ) ;
#33607=CARTESIAN_POINT ( 'NONE',  ( -46.58178904775838447, -24.51419770103157347, 9.386484678747180510 ) ) ;
#33610=EDGE_CURVE ( 'NONE', #82393, #30291, #45530, .T. ) ;
#33611=CARTESIAN_POINT ( 'NONE',  ( 1.624102159173431259, 21.17561035156254334, -1.500000000000002220 ) ) ;
#33615=CARTESIAN_POINT ( 'NONE',  ( -16.21501377034323710, -14.60173171477820198, 11.49999999999998934 ) ) ;
#33616=CARTESIAN_POINT ( 'NONE',  ( -103.5871769483072313, -24.51419770103158058, 9.386484678747171628 ) ) ;
#33619=CARTESIAN_POINT ( 'NONE',  ( -21.72861685410901700, 2.547970858986955189, -1.500000000000002220 ) ) ;
#33621=ORIENTED_EDGE ( 'NONE', *, *, #71674, .F. ) ;
#33623=CARTESIAN_POINT ( 'NONE',  ( -85.63410945799364526, -24.40133493613049964, 9.663955038902802386 ) ) ;
#33626=VECTOR ( 'NONE', #98514, 1000.000000000000114 ) ;
#33629=CARTESIAN_POINT ( 'NONE',  ( -99.62287095715005592, -24.64965695001468404, 8.947790433994178727 ) ) ;
#33633=CARTESIAN_POINT ( 'NONE',  ( -82.64545374615299522, -23.48783264082478084, -1.443836473390069264 ) ) ;
#33634=CARTESIAN_POINT ( 'NONE',  ( 21.10678091372558640, -2.468637549841573797, -1.500000000000002220 ) ) ;
#33635=CARTESIAN_POINT ( 'NONE',  ( -57.52287095715005449, -24.64965694238407323, 8.947790433994201820 ) ) ;
#33636=CARTESIAN_POINT ( 'NONE',  ( -30.61275986115374437, -24.37728322581795481, 9.960208392924579712 ) ) ;
#33637=DIRECTION ( 'NONE',  ( 3.773278334444167608E-23, -1.000000000000000000, 0.000000000000000000 ) ) ;
#33639=CARTESIAN_POINT ( 'NONE',  ( -68.62364069832202063, -24.65952944569304606, 1.056160979905701236 ) ) ;
#33640=CARTESIAN_POINT ( 'NONE',  ( -8.724563080612403709, -17.33930400145671413, -1.500000000000002220 ) ) ;
#33643=CARTESIAN_POINT ( 'NONE',  ( 14.32981562401322506, -13.22600733894156200, 11.49999999999999645 ) ) ;
#33647=EDGE_CURVE ( 'NONE', #59212, #50584, #95117, .T. ) ;
#33648=EDGE_LOOP ( 'NONE', ( #76828, #42809, #59147, #53216 ) ) ;
#33650=CARTESIAN_POINT ( 'NONE',  ( -89.62358325167234341, -24.65952944569304250, 1.056160979905701902 ) ) ;
#33652=CARTESIAN_POINT ( 'NONE',  ( -81.86427935766467101, -25.24813745008903965, 6.429952853325594297 ) ) ;
#33653=CARTESIAN_POINT ( 'NONE',  ( 14.14096853472169535, -13.71769858867784464, 11.49999999999998934 ) ) ;
#33656=CARTESIAN_POINT ( 'NONE',  ( -78.52287095715003318, -23.73907113216987952, -1.053371485793253015 ) ) ;
#33657=CARTESIAN_POINT ( 'NONE',  ( -114.5228709571500616, -23.47596703998600631, 11.44779298504228038 ) ) ;
#33658=EDGE_CURVE ( 'NONE', #61303, #72922, #58821, .T. ) ;
#33660=DIRECTION ( 'NONE',  ( -3.773278334444166432E-23, 1.000000000000000000, 0.000000000000000000 ) ) ;
#33664=CARTESIAN_POINT ( 'NONE',  ( -50.38191529551148307, -29.50248914370730091, 2.832395270851967073 ) ) ;
#33665=CARTESIAN_POINT ( 'NONE',  ( -69.36083545395123906, -25.24515197910791997, 6.029876749600012964 ) ) ;
#33666=CARTESIAN_POINT ( 'NONE',  ( -79.52287095715006160, -24.34917612406836795, 0.1852690917426539075 ) ) ;
#33667=CARTESIAN_POINT ( 'NONE',  ( -13.68957358570155769, -14.46295258127404892, 11.49999999999998934 ) ) ;
#33668=CARTESIAN_POINT ( 'NONE',  ( -75.63647615153271886, -24.40133493613049964, 9.663955038902805939 ) ) ;
#33669=CARTESIAN_POINT ( 'NONE',  ( -19.55781625546462976, 3.520333346782119843, -1.500000000000002220 ) ) ;
#33674=B_SPLINE_CURVE_WITH_KNOTS ( 'NONE', 3,
 ( #70864, #69859, #24664, #62763, #24170, #55644 ),
 .UNSPECIFIED., .F., .F.,
 ( 4, 2, 4 ),
 ( 1.570755371633934808E-05, 0.001396183895866086669, 0.002776660238015834278 ),
 .UNSPECIFIED. ) ;
#33675=CARTESIAN_POINT ( 'NONE',  ( -104.6228709571500559, -23.47596703998600631, 11.44779298504227860 ) ) ;
#33678=CARTESIAN_POINT ( 'NONE',  ( -15.22196369898608737, 14.14466773073655581, 11.49999999999999645 ) ) ;
#33680=ADVANCED_FACE ( 'NONE', ( #82342 ), #40881, .T. ) ;
#33681=CARTESIAN_POINT ( 'NONE',  ( -51.26161549125684758, -25.24476575314045945, 3.786882481863750094 ) ) ;
#33682=CARTESIAN_POINT ( 'NONE',  ( 2.723195454624489642, 22.67993996152103620, 11.49999999999999645 ) ) ;
#33684=B_SPLINE_SURFACE_WITH_KNOTS ( 'NONE', 3, 3, ( 
 ( #74372, #51550, #34321, #90103 ),
 ( #19581, #81989, #28705, #51050 ),
 ( #81495, #28202, #27210, #35816 ),
 ( #96223, #4868, #27708, #96707 ),
 ( #73387, #66790, #98195, #43929 ),
 ( #19080, #12473, #20577, #58654 ),
 ( #82480, #89602, #97708, #3882 ) ),
 .UNSPECIFIED., .F., .F., .F.,
 ( 4, 3, 4 ),
 ( 4, 4 ),
 ( 0.7945040050992233649, 0.8970133687736495665, 0.9995227324480757680 ),
 ( 0.1695370789669584655, 0.1706280730879164986 ),
 .UNSPECIFIED. ) ;
#33685=CARTESIAN_POINT ( 'NONE',  ( -54.62287095715005592, -23.47593901973091235, -1.443836447539009749 ) ) ;
#33686=CARTESIAN_POINT ( 'NONE',  ( -127.5906365579869970, -23.48783264082477018, -1.443836473390083919 ) ) ;
#33687=EDGE_LOOP ( 'NONE', ( #30755, #48886, #39166, #34112 ) ) ;
#33688=CARTESIAN_POINT ( 'NONE',  ( -14.42758394406654610, -14.16023863206117994, 11.49999999999998934 ) ) ;
#33689=CARTESIAN_POINT ( 'NONE',  ( -89.62287095715004170, -23.47596703998600631, 11.44779298504227860 ) ) ;
#33692=CARTESIAN_POINT ( 'NONE',  ( -100.6228709571500559, -23.48783264082478794, -1.443836473390061936 ) ) ;
#33693=B_SPLINE_CURVE_WITH_KNOTS ( 'NONE', 3,
 ( #2114, #25933, #57905, #72124 ),
 .UNSPECIFIED., .F., .F.,
 ( 4, 4 ),
 ( 0.000000000000000000, 9.999999999998897304E-05 ),
 .UNSPECIFIED. ) ;
#33694=ORIENTED_EDGE ( 'NONE', *, *, #25362, .F. ) ;
#33695=CARTESIAN_POINT ( 'NONE',  ( -45.62287095715004881, -29.50248789122583659, 2.256150453626215580 ) ) ;
#33696=CARTESIAN_POINT ( 'NONE',  ( -100.6228709571500843, -24.51163499207179441, 0.6490370598555492698 ) ) ;
#33697=CARTESIAN_POINT ( 'NONE',  ( 8.874027960929927517, 17.90919871486395465, -1.500000000000002220 ) ) ;
#33698=CARTESIAN_POINT ( 'NONE',  ( -11.48448384864204996, -17.54081393385053644, 11.49999999999999645 ) ) ;
#33701=CARTESIAN_POINT ( 'NONE',  ( 19.60348439636399931, 10.09110264789753053, 11.49999999999998934 ) ) ;
#33703=CARTESIAN_POINT ( 'NONE',  ( -53.55620429048338593, -24.64965694238574656, 8.947790433994208925 ) ) ;
#33705=CARTESIAN_POINT ( 'NONE',  ( -127.5228709571500616, -23.48786465467242479, 11.44779295918253581 ) ) ;
#33706=CARTESIAN_POINT ( 'NONE',  ( -129.6228709571500417, -29.50248528299804818, 1.056150453629047137 ) ) ;
#33707=CARTESIAN_POINT ( 'NONE',  ( -72.60175781541748563, -23.73766607897670156, -1.055555164236458454 ) ) ;
#33708=ORIENTED_EDGE ( 'NONE', *, *, #42038, .F. ) ;
#33711=AXIS2_PLACEMENT_3D ( 'NONE', #55869, #26899, #73087 ) ;
#33712=ORIENTED_EDGE ( 'NONE', *, *, #47750, .T. ) ;
#33715=DIRECTION ( 'NONE',  ( -3.773278334453080206E-23, 0.9999999999976377785, 2.173523156925979975E-06 ) ) ;
#33716=CARTESIAN_POINT ( 'NONE',  ( 15.43701773751798001, -13.56989305476470875, -1.500000000000002220 ) ) ;
#33718=CARTESIAN_POINT ( 'NONE',  ( -51.62287095715005592, -29.50248528299804818, 1.056150453629033370 ) ) ;
#33720=LINE ( 'NONE', #25603, #36675 ) ;
#33721=CARTESIAN_POINT ( 'NONE',  ( -1.228339276683141579, -22.28195500894762660, 11.49999999999998934 ) ) ;
#33723=CARTESIAN_POINT ( 'NONE',  ( -35.62287095715005592, -29.50248789122583659, 2.256150453626215580 ) ) ;
#33728=CARTESIAN_POINT ( 'NONE',  ( 20.34438994040483806, -4.565235006643893811, 11.49999999999998934 ) ) ;
#33730=CARTESIAN_POINT ( 'NONE',  ( -61.62287095715004881, -23.47596703998600631, 11.44779298504227505 ) ) ;
#33731=EDGE_LOOP ( 'NONE', ( #22194, #19878, #97373, #73025 ) ) ;
#33733=CARTESIAN_POINT ( 'NONE',  ( -69.03624148920614800, -25.25935168378925866, 6.724186225230494252 ) ) ;
#33734=CARTESIAN_POINT ( 'NONE',  ( 7.388015978253313243, 19.69965359013245632, -1.500000000000002220 ) ) ;
#33736=CARTESIAN_POINT ( 'NONE',  ( -114.5228709571500616, -23.48783264083396105, -1.443836473375806895 ) ) ;
#33737=PLANE ( 'NONE',  #56368 ) ;
#33739=FACE_OUTER_BOUND ( 'NONE', #40198, .T. ) ;
#33740=B_SPLINE_CURVE_WITH_KNOTS ( 'NONE', 3,
 ( #73392, #65303, #11478, #58169 ),
 .UNSPECIFIED., .F., .F.,
 ( 4, 4 ),
 ( 6.276132038432468235E-06, 0.001058024727852768581 ),
 .UNSPECIFIED. ) ;
#33741=CARTESIAN_POINT ( 'NONE',  ( -86.62607985270027200, -24.51419770103155926, 9.386484678747176957 ) ) ;
#33742=CARTESIAN_POINT ( 'NONE',  ( -73.58953762381673869, -24.65952944569304606, 1.056160979905698794 ) ) ;
#33743=CARTESIAN_POINT ( 'NONE',  ( 5.343276940429747768, -21.04383479052346217, -1.500000000000002220 ) ) ;
#33744=CARTESIAN_POINT ( 'NONE',  ( -64.52287095715009002, -24.33927499327855770, 9.819080762295815390 ) ) ;
#33745=CARTESIAN_POINT ( 'NONE',  ( -4.481184387785930312, -21.81124396384582909, 11.49999999999999645 ) ) ;
#33746=ORIENTED_EDGE ( 'NONE', *, *, #13130, .T. ) ;
#33747=CARTESIAN_POINT ( 'NONE',  ( -51.52443300084429723, -25.24728917589673216, 6.090565017594450126 ) ) ;
#33752=EDGE_CURVE ( 'NONE', #30676, #100208, #16828, .T. ) ;
#33753=CARTESIAN_POINT ( 'NONE',  ( -110.6228709571500559, -29.50249982740957577, 7.747779886224967605 ) ) ;
#33754=VERTEX_POINT ( 'NONE', #77710 ) ;
#33755=EDGE_LOOP ( 'NONE', ( #93356, #45490, #50401, #64120 ) ) ;
#33757=DIRECTION ( 'NONE',  ( -3.773278334453079618E-23, 0.9999999999976377785, 2.173523156925979975E-06 ) ) ;
#33758=CARTESIAN_POINT ( 'NONE',  ( -35.52287095715007581, -24.62226745350439217, 0.9660975649728085202 ) ) ;
#33760=ORIENTED_EDGE ( 'NONE', *, *, #71363, .T. ) ;
#33761=CARTESIAN_POINT ( 'NONE',  ( -130.5728709571500588, -25.39039004847436232, 5.722739179073901283 ) ) ;
#33762=CARTESIAN_POINT ( 'NONE',  ( -22.26391555059773353, 2.265117081278330780, -1.500000000000002220 ) ) ;
#33765=CARTESIAN_POINT ( 'NONE',  ( -34.52287095715006160, -24.33927499327853994, 9.819080762295811837 ) ) ;
#33767=PLANE ( 'NONE',  #78207 ) ;
#33770=CARTESIAN_POINT ( 'NONE',  ( -130.5728709571500588, -24.82959736273287632, 8.370978854367631783 ) ) ;
#33771=CARTESIAN_POINT ( 'NONE',  ( -15.85469643196389278, -11.46343829903102396, -1.500000000000002220 ) ) ;
#33772=CARTESIAN_POINT ( 'NONE',  ( -49.50841769935765768, -25.27292115247390569, 3.984447733149576898 ) ) ;
#33773=ORIENTED_EDGE ( 'NONE', *, *, #55304, .F. ) ;
#33774=CARTESIAN_POINT ( 'NONE',  ( 2.436486579176012413, 21.40072447632485364, -1.500000000000002220 ) ) ;
#33775=CARTESIAN_POINT ( 'NONE',  ( -64.52287095715006160, -29.50250786944525672, 11.44777988621623876 ) ) ;
#33776=CARTESIAN_POINT ( 'NONE',  ( -119.5895376238167245, -23.47596703998600631, 11.44779298504227683 ) ) ;
#33779=CARTESIAN_POINT ( 'NONE',  ( 21.34038654641452482, 8.310931564070170197, -1.500000000000002220 ) ) ;
#33781=CARTESIAN_POINT ( 'NONE',  ( -39.62287095715005592, -29.50248528299804818, 1.056150453629031594 ) ) ;
#33783=CARTESIAN_POINT ( 'NONE',  ( -18.39468835979788608, -8.022455445098881199, 11.49999999999999645 ) ) ;
#33785=DIRECTION ( 'NONE',  ( -3.773278334453079618E-23, 0.9999999999976377785, 2.173523156925979975E-06 ) ) ;
#33787=DIRECTION ( 'NONE',  ( 0.000000000000000000, 2.173523156925980399E-06, -0.9999999999976378895 ) ) ;
#33789=CARTESIAN_POINT ( 'NONE',  ( -126.5228709571500616, -24.64965694238408034, 8.947790433994189385 ) ) ;
#33790=CARTESIAN_POINT ( 'NONE',  ( 9.833179757865110560, 17.22857952739193266, 11.49999999999998934 ) ) ;
#33792=CARTESIAN_POINT ( 'NONE',  ( 11.96684523812195700, 15.63349346248531546, -1.500000000000002220 ) ) ;
#33793=CARTESIAN_POINT ( 'NONE',  ( -42.59367499821067327, -24.15543982623907127, -0.2315651400026575435 ) ) ;
#33799=CARTESIAN_POINT ( 'NONE',  ( 19.39950376024442846, -7.079068461131618584, 11.49999999999999645 ) ) ;
#33803=CARTESIAN_POINT ( 'NONE',  ( -19.18631400275845422, -11.98935526391121087, 11.49999999999999645 ) ) ;
#33805=ADVANCED_FACE ( 'NONE', ( #8726 ), #85843, .F. ) ;
#33806=CARTESIAN_POINT ( 'NONE',  ( -72.62287095715005592, -29.50248528299804818, 1.056150453629036701 ) ) ;
#33807=CARTESIAN_POINT ( 'NONE',  ( -97.55776836362488780, -23.73766607897671221, -1.055555164236451793 ) ) ;
#33808=CARTESIAN_POINT ( 'NONE',  ( -26.76727616692972234, -24.79064461044202616, 2.646210252706996169 ) ) ;
#33809=CARTESIAN_POINT ( 'NONE',  ( -26.85174826923451974, -24.93063591732613204, 8.053059820581612627 ) ) ;
#33812=CARTESIAN_POINT ( 'NONE',  ( -79.57226238056755108, -25.31596297220300329, 5.312438930566553807 ) ) ;
#33813=CARTESIAN_POINT ( 'NONE',  ( 9.452765381649220089, 20.79790602042944414, 11.49999999999998934 ) ) ;
#33815=CARTESIAN_POINT ( 'NONE',  ( -91.52287095715006160, -23.47593901973090524, -1.443836447538996648 ) ) ;
#33816=FACE_OUTER_BOUND ( 'NONE', #56436, .T. ) ;
#33817=CARTESIAN_POINT ( 'NONE',  ( 14.28312119630281174, -17.39864199977734671, 11.49999999999999645 ) ) ;
#33818=ORIENTED_EDGE ( 'NONE', *, *, #56665, .T. ) ;
#33819=CARTESIAN_POINT ( 'NONE',  ( -43.54651782967658136, -24.15543982623906771, -0.2315651400026568496 ) ) ;
#33820=CARTESIAN_POINT ( 'NONE',  ( -20.58003014649542095, 7.718188279156099618, -1.500000000000002220 ) ) ;
#33823=CARTESIAN_POINT ( 'NONE',  ( -29.24573430514233507, -24.79699791941041553, 5.187749665486013129 ) ) ;
#33825=CARTESIAN_POINT ( 'NONE',  ( -48.63354421635416003, -24.35071581493542681, 9.817618358456027039 ) ) ;
#33827=ORIENTED_EDGE ( 'NONE', *, *, #38960, .T. ) ;
#33828=CARTESIAN_POINT ( 'NONE',  ( -54.59312836098206390, -24.15620529776628089, 10.23563542870661180 ) ) ;
#33829=CARTESIAN_POINT ( 'NONE',  ( 14.40702264168333890, -14.58922348230443689, -1.500000000000002220 ) ) ;
#33830=ORIENTED_EDGE ( 'NONE', *, *, #44876, .T. ) ;
#33832=ORIENTED_EDGE ( 'NONE', *, *, #52311, .F. ) ;
#33834=CARTESIAN_POINT ( 'NONE',  ( -72.52287095715007581, -23.47593901973090169, -1.443836447538996870 ) ) ;
#33835=CARTESIAN_POINT ( 'NONE',  ( 16.03631736716203449, -16.64276770305488284, 11.49999999999998934 ) ) ;
#33836=CARTESIAN_POINT ( 'NONE',  ( -104.5511856791031562, -24.35071581493544102, 9.817618358456019934 ) ) ;
#33837=CARTESIAN_POINT ( 'NONE',  ( -7.038884989605349141, -19.10714869031923513, -1.500000000000002220 ) ) ;
#33841=CARTESIAN_POINT ( 'NONE',  ( -51.69051972431498143, -25.25860399288287894, 3.823735972406262729 ) ) ;
#33842=ADVANCED_FACE ( 'NONE', ( #17328 ), #75059, .T. ) ;
#33843=CARTESIAN_POINT ( 'NONE',  ( -93.62287095715011276, -23.95044443724992789, 10.65354141964649592 ) ) ;
#33845=EDGE_LOOP ( 'NONE', ( #55554, #96742, #70898, #78339 ) ) ;
#33846=CARTESIAN_POINT ( 'NONE',  ( -27.75618988833547718, -24.76880854971131996, 2.278559976844410695 ) ) ;
#33848=ORIENTED_EDGE ( 'NONE', *, *, #30963, .F. ) ;
#33850=B_SPLINE_CURVE_WITH_KNOTS ( 'NONE', 3,
 ( #37791, #67758, #99174, #7323 ),
 .UNSPECIFIED., .F., .F.,
 ( 4, 4 ),
 ( 0.000000000000000000, 1.000000000000000000 ),
 .UNSPECIFIED. ) ;
#33851=CARTESIAN_POINT ( 'NONE',  ( 10.28901978357889035, -18.02705789925236957, 11.49999999999998934 ) ) ;
#33856=DIRECTION ( 'NONE',  ( 0.000000000000000000, -0.9999999999976377785, -2.173523156925979975E-06 ) ) ;
#33857=EDGE_LOOP ( 'NONE', ( #65966, #41345, #99673, #39600 ) ) ;
#33859=CARTESIAN_POINT ( 'NONE',  ( -29.62287095715004881, -23.64899563800052817, -1.053577770480854436 ) ) ;
#33863=CARTESIAN_POINT ( 'NONE',  ( -28.59316516807098196, -24.74616672227249481, 1.851678086324305861 ) ) ;
#33864=CARTESIAN_POINT ( 'NONE',  ( 18.18892703665305177, -12.56521834855340281, 11.49999999999999645 ) ) ;
#33865=VERTEX_POINT ( 'NONE', #96455 ) ;
#33866=CARTESIAN_POINT ( 'NONE',  ( -108.5964263034907873, -23.48783264082478794, -1.443836473390062825 ) ) ;
#33867=EDGE_CURVE ( 'NONE', #90247, #80731, #30948, .T. ) ;
#33868=CARTESIAN_POINT ( 'NONE',  ( -18.09186581907994196, -13.49991075323410250, -1.500000000000002220 ) ) ;
#33870=DIRECTION ( 'NONE',  ( -3.773278334453080206E-23, 0.9999999999976377785, 2.173523156925979975E-06 ) ) ;
#33871=EDGE_LOOP ( 'NONE', ( #95171, #26022, #74620, #7763 ) ) ;
#33873=VERTEX_POINT ( 'NONE', #65538 ) ;
#33874=ADVANCED_FACE ( 'NONE', ( #42689 ), #85687, .T. ) ;
#33875=CARTESIAN_POINT ( 'NONE',  ( -127.5228709571500616, -23.47593901973090524, -1.443836447538996204 ) ) ;
#33879=CARTESIAN_POINT ( 'NONE',  ( 4.708956132399880978, 20.65895737721473679, -1.500000000000002220 ) ) ;
#33881=CARTESIAN_POINT ( 'NONE',  ( -32.62287095715006302, -23.47596703998600276, 11.44779298504227505 ) ) ;
#33882=LINE ( 'NONE', #33373, #89180 ) ;
#33883=CARTESIAN_POINT ( 'NONE',  ( -17.21897301287555848, -14.04741862099043104, -1.500000000000002220 ) ) ;
#33884=CARTESIAN_POINT ( 'NONE',  ( -114.5584126538706045, -23.48783264082478794, -1.443836473390062380 ) ) ;
#33885=EDGE_CURVE ( 'NONE', #42129, #34509, #62416, .T. ) ;
#33887=CARTESIAN_POINT ( 'NONE',  ( -29.62287095715004881, -29.50247984919044697, -1.443849411171584940 ) ) ;
#33888=CARTESIAN_POINT ( 'NONE',  ( -50.55620429048339304, -23.47596703998600276, 11.44779298504227505 ) ) ;
#33890=CARTESIAN_POINT ( 'NONE',  ( -49.52287095715004739, -24.66019654487198665, 8.947790411086131712 ) ) ;
#33891=CARTESIAN_POINT ( 'NONE',  ( -19.46337940159461866, -0.4807646128305608779, -1.500000000000002220 ) ) ;
#33892=CARTESIAN_POINT ( 'NONE',  ( 21.36505145794347982, 1.902718533054148509, 11.49999999999998934 ) ) ;
#33893=CARTESIAN_POINT ( 'NONE',  ( -85.52287095715004739, -24.99156044556120193, 7.747789690856173195 ) ) ;
#33895=FACE_OUTER_BOUND ( 'NONE', #54339, .T. ) ;
#33897=CARTESIAN_POINT ( 'NONE',  ( -22.42851769774927817, -3.676000928666301792, -1.500000000000002220 ) ) ;
#33898=B_SPLINE_CURVE_WITH_KNOTS ( 'NONE', 3,
 ( #41029, #3470, #57756, #33907, #42535, #71982 ),
 .UNSPECIFIED., .F., .F.,
 ( 4, 2, 4 ),
 ( 0.000000000000000000, 0.001380901958385395700, 0.002761803916770791401 ),
 .UNSPECIFIED. ) ;
#33900=CARTESIAN_POINT ( 'NONE',  ( -102.5170246378254149, -23.96119346886881729, -0.6495511937831880411 ) ) ;
#33902=CARTESIAN_POINT ( 'NONE',  ( -1.646307629438301667, 19.86461321233117872, 11.49999999999999645 ) ) ;
#33903=CARTESIAN_POINT ( 'NONE',  ( -104.6250152058018870, -24.51314013834316796, 0.6176544820404187286 ) ) ;
#33906=B_SPLINE_CURVE_WITH_KNOTS ( 'NONE', 3,
 ( #22610, #38854, #7397, #99733, #61219, #38356, #16010, #23614, #293, #92138, #14011, #85525, #8405, #39357, #70315, #53604, #75911, #53101, #69308, #6416 ),
 .UNSPECIFIED., .F., .F.,
 ( 4, 2, 2, 2, 2, 2, 2, 2, 2, 4 ),
 ( 0.000000000000000000, 0.0008691610528771086383, 0.001303741579315663337, 0.001738322105754218144, 0.002172902632192772517, 0.002390192895412054149, 0.002607483158631335781, 0.003042063685069898177, 0.003259353948289179376, 0.003476644211508461008 ),
 .UNSPECIFIED. ) ;
#33907=CARTESIAN_POINT ( 'NONE',  ( -128.5228709571499621, -23.95044443724993144, 10.65354141964648704 ) ) ;
#33908=CARTESIAN_POINT ( 'NONE',  ( -118.6228709571500559, -23.47593901973091235, -1.443836447538997536 ) ) ;
#33909=ORIENTED_EDGE ( 'NONE', *, *, #70970, .F. ) ;
#33910=DIRECTION ( 'NONE',  ( -1.000000000000000000, -3.773278334444167608E-23, -8.201307833595939069E-29 ) ) ;
#33912=CARTESIAN_POINT ( 'NONE',  ( -14.64807036877012258, -15.96857234361563904, 11.49999999999998934 ) ) ;
#33913=CARTESIAN_POINT ( 'NONE',  ( -51.91883209273765232, -25.23905552336719182, 6.365853120814609412 ) ) ;
#33915=CARTESIAN_POINT ( 'NONE',  ( 9.662506626059768067, -16.94115208737379774, -1.500000000000002220 ) ) ;
#33922=CARTESIAN_POINT ( 'NONE',  ( -59.62287095715004881, -24.64965695001468404, 8.947790433994185832 ) ) ;
#33923=CARTESIAN_POINT ( 'NONE',  ( 0.3735783541106268979, -20.45636175344465713, 11.49999999999999645 ) ) ;
#33926=CARTESIAN_POINT ( 'NONE',  ( -101.5468792378191978, -25.24282061761980955, 6.236250683194342059 ) ) ;
#33927=ORIENTED_EDGE ( 'NONE', *, *, #17913, .T. ) ;
#33928=CARTESIAN_POINT ( 'NONE',  ( -55.52287095715006870, -23.48786465467241058, 11.44779295918254824 ) ) ;
#33931=CARTESIAN_POINT ( 'NONE',  ( -49.29568538784691611, -25.31439443837986403, 5.964271667760576712 ) ) ;
#33932=B_SPLINE_CURVE_WITH_KNOTS ( 'NONE', 3,
 ( #99798, #30305, #60780, #84095, #61283, #46542, #69376, #360 ),
 .UNSPECIFIED., .F., .F.,
 ( 4, 2, 2, 4 ),
 ( -0.001240355328176665156, -0.0002398155169398032398, 0.0007607242942970586768, 0.002761803916770783594 ),
 .UNSPECIFIED. ) ;
#33933=CARTESIAN_POINT ( 'NONE',  ( -109.5552946845191826, -23.96119346886880663, -0.6495511937832053606 ) ) ;
#33934=ORIENTED_EDGE ( 'NONE', *, *, #26422, .F. ) ;
#33935=CARTESIAN_POINT ( 'NONE',  ( -66.52209599655327565, -23.48786465467241058, 11.44779295918254824 ) ) ;
#33936=CARTESIAN_POINT ( 'NONE',  ( -8.204236019480731557, -21.45505762417899831, 11.49999999999999645 ) ) ;
#33937=CARTESIAN_POINT ( 'NONE',  ( 16.48639501038195121, -15.69157857782056276, -1.500000000000002220 ) ) ;
#33940=CARTESIAN_POINT ( 'NONE',  ( -90.64148924035946209, -23.85016227208580730, -0.8807180028928307536 ) ) ;
#33941=CARTESIAN_POINT ( 'NONE',  ( -74.52287095715010423, -23.96177878511308279, 10.65340807706329684 ) ) ;
#33943=CARTESIAN_POINT ( 'NONE',  ( -21.72861685410901700, 2.547970858986955189, -1.500000000000002220 ) ) ;
#33945=CARTESIAN_POINT ( 'NONE',  ( -69.62708888908201743, -24.51419770103157347, 9.386484678747178734 ) ) ;
#33947=CARTESIAN_POINT ( 'NONE',  ( -48.87835844652435213, -25.27427334345122034, 6.006362479330361381 ) ) ;
#33948=CARTESIAN_POINT ( 'NONE',  ( -120.6228709571500417, -24.51163499207180507, 0.6490370598555501580 ) ) ;
#33949=CARTESIAN_POINT ( 'NONE',  ( -34.55620429048339304, -24.65952944569303895, 1.056160979905690356 ) ) ;
#33950=ORIENTED_EDGE ( 'NONE', *, *, #28553, .T. ) ;
#33951=CARTESIAN_POINT ( 'NONE',  ( -10.82153711268468932, 17.32902648900640230, 11.49999999999998934 ) ) ;
#33954=CARTESIAN_POINT ( 'NONE',  ( 22.97298546869389568, 1.202750762487129199, 11.49999999999998934 ) ) ;
#33955=CARTESIAN_POINT ( 'NONE',  ( -105.5228709571501042, -23.48783264082477018, -1.443836473390085917 ) ) ;
#33957=DIRECTION ( 'NONE',  ( 0.000000000000000000, -0.9999999999976377785, -2.173523156925979128E-06 ) ) ;
#33958=CARTESIAN_POINT ( 'NONE',  ( -77.92287095715008149, -23.47596703998600631, 11.44779298504227683 ) ) ;
#33959=CARTESIAN_POINT ( 'NONE',  ( -122.6228709571500417, -24.66019654487199730, 8.947790411086121054 ) ) ;
#33961=CARTESIAN_POINT ( 'NONE',  ( -1.966620079519992181, -21.27258529651320274, 11.49999999999999645 ) ) ;
#33962=ORIENTED_EDGE ( 'NONE', *, *, #57419, .F. ) ;
#33963=ORIENTED_EDGE ( 'NONE', *, *, #91391, .F. ) ;
#33964=CARTESIAN_POINT ( 'NONE',  ( -17.21897301287555848, -14.04741862099043104, 11.49999999999998934 ) ) ;
#33965=CARTESIAN_POINT ( 'NONE',  ( -18.22997975830956108, -9.740667652671243459, -1.500000000000002220 ) ) ;
#33967=VERTEX_POINT ( 'NONE', #86673 ) ;
#33968=FACE_OUTER_BOUND ( 'NONE', #69316, .T. ) ;
#33970=ORIENTED_EDGE ( 'NONE', *, *, #8029, .T. ) ;
#33973=ORIENTED_EDGE ( 'NONE', *, *, #9904, .T. ) ;
#33974=CARTESIAN_POINT ( 'NONE',  ( -111.5122638532038053, -25.28710546256126435, 4.332404433089555695 ) ) ;
#33975=CARTESIAN_POINT ( 'NONE',  ( -5.628781154649386664, 20.11113626451368219, -1.500000000000002220 ) ) ;
#33976=EDGE_CURVE ( 'NONE', #100229, #61899, #34559, .T. ) ;
#33977=B_SPLINE_CURVE_WITH_KNOTS ( 'NONE', 3,
 ( #98387, #29887, #97887, #5548 ),
 .UNSPECIFIED., .F., .F.,
 ( 4, 4 ),
 ( 0.000000000000000000, 1.000000000000000000 ),
 .UNSPECIFIED. ) ;
#33978=CARTESIAN_POINT ( 'NONE',  ( 11.09338859787202480, -18.89396691112096605, 11.49999999999999645 ) ) ;
#33981=CARTESIAN_POINT ( 'NONE',  ( 12.95044643391442030, 18.39415735498938176, 11.49999999999998934 ) ) ;
#33982=VECTOR ( 'NONE', #87026, 1000.000000000000114 ) ;
#33983=CARTESIAN_POINT ( 'NONE',  ( 20.88312143257166653, -1.666129412636018214, 11.49999999999998934 ) ) ;
#33984=CARTESIAN_POINT ( 'NONE',  ( -38.62894216554127524, -24.51314013834316086, 0.6176544820404135105 ) ) ;
#33987=ORIENTED_EDGE ( 'NONE', *, *, #29372, .T. ) ;
#33988=AXIS2_PLACEMENT_3D ( 'NONE', #22445, #7231, #38178 ) ;
#33989=B_SPLINE_CURVE_WITH_KNOTS ( 'NONE', 3,
 ( #51762, #35543, #66513, #27917 ),
 .UNSPECIFIED., .F., .F.,
 ( 4, 4 ),
 ( 0.000000000000000000, 1.000000000000000000 ),
 .UNSPECIFIED. ) ;
#33991=ORIENTED_EDGE ( 'NONE', *, *, #58990, .F. ) ;
#33992=VECTOR ( 'NONE', #9348, 1000.000000000000114 ) ;
#33995=CARTESIAN_POINT ( 'NONE',  ( -52.53663968116620708, -24.51314013834315375, 0.6176544820404114011 ) ) ;
#33996=ORIENTED_EDGE ( 'NONE', *, *, #76326, .T. ) ;
#33998=CARTESIAN_POINT ( 'NONE',  ( -11.90495014755217618, 17.82271480561356469, -1.500000000000002220 ) ) ;
#33999=ORIENTED_EDGE ( 'NONE', *, *, #80310, .F. ) ;
#34001=CARTESIAN_POINT ( 'NONE',  ( 17.50165659415881336, 11.77592616506222711, -1.500000000000002220 ) ) ;
#34002=CARTESIAN_POINT ( 'NONE',  ( -30.51821473474449675, -25.31108805091020741, 6.147639284700202822 ) ) ;
#34004=CARTESIAN_POINT ( 'NONE',  ( -50.50115682139630735, -24.15602025860895097, 10.28564288303536856 ) ) ;
#34005=CARTESIAN_POINT ( 'NONE',  ( -101.5869946791053025, -24.51314013834316086, 0.6176544820404198388 ) ) ;
#34006=DIRECTION ( 'NONE',  ( -3.773278334444166432E-23, 1.000000000000000000, 0.000000000000000000 ) ) ;
#34007=CARTESIAN_POINT ( 'NONE',  ( -16.14483305390557888, 14.99321182834783528, -1.500000000000002220 ) ) ;
#34008=ORIENTED_EDGE ( 'NONE', *, *, #88791, .T. ) ;
#34009=CARTESIAN_POINT ( 'NONE',  ( -116.5555276665938180, -23.96119346886881729, -0.6495511937831834892 ) ) ;
#34010=ADVANCED_FACE ( 'NONE', ( #77547 ), #24277, .T. ) ;
#34012=CARTESIAN_POINT ( 'NONE',  ( -41.14436886340001820, -25.27956039219115425, 5.395510761495216023 ) ) ;
#34013=CARTESIAN_POINT ( 'NONE',  ( -26.94908181867664965, -25.04135458203152353, 6.075536601959949934 ) ) ;
#34014=DIRECTION ( 'NONE',  ( 0.000000000000000000, -2.173523156925980399E-06, 0.9999999999976378895 ) ) ;
#34016=CARTESIAN_POINT ( 'NONE',  ( 2.936642053869352953, -21.15864249054145674, -1.500000000000002220 ) ) ;
#34019=CARTESIAN_POINT ( 'NONE',  ( -64.53585642586003246, -24.66019654487199730, 8.947790411086113949 ) ) ;
#34020=CARTESIAN_POINT ( 'NONE',  ( -79.52287095715006160, -29.50250243563736774, 8.947779886222141599 ) ) ;
#34021=CARTESIAN_POINT ( 'NONE',  ( 22.10748686624256720, -4.471405416651531795, -1.500000000000002220 ) ) ;
#34024=B_SPLINE_CURVE_WITH_KNOTS ( 'NONE', 3,
 ( #63552, #50195, #94472, #19231 ),
 .UNSPECIFIED., .F., .F.,
 ( 4, 4 ),
 ( 0.5108647960461032422, 0.5198712273182189980 ),
 .UNSPECIFIED. ) ;
#34026=CARTESIAN_POINT ( 'NONE',  ( -120.6228709571500417, -23.47596703998600631, 11.44779298504227683 ) ) ;
#34027=CARTESIAN_POINT ( 'NONE',  ( -16.18664964019209052, -11.25563402961023662, 11.49999999999999645 ) ) ;
#34028=PLANE ( 'NONE',  #87726 ) ;
#34031=VERTEX_POINT ( 'NONE', #48635 ) ;
#34032=B_SPLINE_CURVE_WITH_KNOTS ( 'NONE', 3,
 ( #15067, #60269, #46035, #54155, #76956, #85078, #91192, #23671, #77454, #16059 ),
 .UNSPECIFIED., .F., .F.,
 ( 4, 2, 2, 2, 4 ),
 ( 0.000000000000000000, 0.0007250860325595927204, 0.001087629048839393146, 0.001268900556979295907, 0.001450172065119198668 ),
 .UNSPECIFIED. ) ;
#34035=CARTESIAN_POINT ( 'NONE',  ( -105.5228709571501184, -24.63345952396258198, 9.038047939301510070 ) ) ;
#34036=CARTESIAN_POINT ( 'NONE',  ( -20.54952838774410750, 6.582847151591199264, 11.49999999999998934 ) ) ;
#34037=CARTESIAN_POINT ( 'NONE',  ( -90.92287095715005307, -23.47593901973090169, -1.443836447538996870 ) ) ;
#34038=CARTESIAN_POINT ( 'NONE',  ( -76.58953762381673869, -24.66019654487198665, 8.947790411086133489 ) ) ;
#34040=CARTESIAN_POINT ( 'NONE',  ( -97.62287095715008434, -23.47596703998600631, 11.44779298504227860 ) ) ;
#34041=CARTESIAN_POINT ( 'NONE',  ( -16.30015253881794379, -11.17962500214296639, 11.49999999999998934 ) ) ;
#34044=CARTESIAN_POINT ( 'NONE',  ( 6.837353022973060135, 19.10023500134885310, 11.49999999999999645 ) ) ;
#34046=VECTOR ( 'NONE', #90489, 1000.000000000000114 ) ;
#34051=CARTESIAN_POINT ( 'NONE',  ( -48.62287095715004881, -29.50248528299804818, 1.056150453629033370 ) ) ;
#34055=PLANE ( 'NONE',  #2547 ) ;
#34056=CARTESIAN_POINT ( 'NONE',  ( 18.34943919012036773, 8.063251210807163005, 11.49999999999998934 ) ) ;
#34060=VECTOR ( 'NONE', #32862, 1000.000000000000114 ) ;
#34062=CARTESIAN_POINT ( 'NONE',  ( -35.62380676451632411, -25.00158670708910336, 2.256160236439224143 ) ) ;
#34063=CARTESIAN_POINT ( 'NONE',  ( -80.08697634283775812, -25.30560378225014873, 5.004156656408841997 ) ) ;
#34065=FACE_OUTER_BOUND ( 'NONE', #81626, .T. ) ;
#34066=CARTESIAN_POINT ( 'NONE',  ( -73.60155033630429955, -23.73766607897670511, -1.055555164236457344 ) ) ;
#34067=EDGE_CURVE ( 'NONE', #234, #39724, #85398, .T. ) ;
#34070=VECTOR ( 'NONE', #64888, 1000.000000000000114 ) ;
#34071=CARTESIAN_POINT ( 'NONE',  ( -98.87540794031171743, -25.20650842489795807, 6.812665538484692362 ) ) ;
#34072=VERTEX_POINT ( 'NONE', #23769 ) ;
#34074=CARTESIAN_POINT ( 'NONE',  ( -0.6891947355827284794, 20.32259304938107292, -1.500000000000002220 ) ) ;
#34076=CARTESIAN_POINT ( 'NONE',  ( -32.53790792079495020, -24.34968618360933590, 0.1864209137778856384 ) ) ;
#34077=CARTESIAN_POINT ( 'NONE',  ( -118.5228709571500758, -23.47596703998600631, 11.44779298504227860 ) ) ;
#34080=CARTESIAN_POINT ( 'NONE',  ( -59.61137031377487006, -23.48786465467240703, 11.44779295918255180 ) ) ;
#34082=CARTESIAN_POINT ( 'NONE',  ( -49.39546678031889826, -25.26264066864941782, 6.587942125045247899 ) ) ;
#34083=CARTESIAN_POINT ( 'NONE',  ( -30.47287095715008576, -24.67388046057699924, 1.121487310756236200 ) ) ;
#34084=CARTESIAN_POINT ( 'NONE',  ( 12.26186175617451113, -17.30295086655154080, 11.49999999999999645 ) ) ;
#34085=EDGE_CURVE ( 'NONE', #2532, #80762, #62868, .T. ) ;
#34086=CARTESIAN_POINT ( 'NONE',  ( -0.9539927174334467130, 22.11892580961223587, -1.500000000000002220 ) ) ;
#34087=CARTESIAN_POINT ( 'NONE',  ( 20.45670835789597319, 2.398913822417158226, 11.49999999999998934 ) ) ;
#34088=VERTEX_POINT ( 'NONE', #47628 ) ;
#34089=CARTESIAN_POINT ( 'NONE',  ( -91.55620429048339304, -23.47596703998600631, 11.44779298504227683 ) ) ;
#34090=VERTEX_POINT ( 'NONE', #94281 ) ;
#34092=FACE_OUTER_BOUND ( 'NONE', #9462, .T. ) ;
#34093=EDGE_LOOP ( 'NONE', ( #90581, #45811, #97977, #22940 ) ) ;
#34094=VERTEX_POINT ( 'NONE', #55748 ) ;
#34095=EDGE_LOOP ( 'NONE', ( #13888, #70181, #6903, #4236 ) ) ;
#34097=B_SPLINE_CURVE_WITH_KNOTS ( 'NONE', 3,
 ( #27717, #65801, #58175, #59169, #28715, #59676 ),
 .UNSPECIFIED., .F., .F.,
 ( 4, 2, 4 ),
 ( 1.570887131795109485E-05, 0.001396322306279764325, 0.002776935741241577573 ),
 .UNSPECIFIED. ) ;
#34100=CARTESIAN_POINT ( 'NONE',  ( -11.67826063220891086, 17.12864047899337550, -1.500000000000002220 ) ) ;
#34102=CARTESIAN_POINT ( 'NONE',  ( -17.53059066697263546, 12.75712217820542627, 11.49999999999999645 ) ) ;
#34105=CARTESIAN_POINT ( 'NONE',  ( -109.5228709571500616, -23.48786465467242479, 11.44779295918253936 ) ) ;
#34106=CARTESIAN_POINT ( 'NONE',  ( 15.34105849444754455, 16.31744944422920440, 11.49999999999998934 ) ) ;
#34108=CARTESIAN_POINT ( 'NONE',  ( -65.65276470879786075, -23.85016227208580730, -0.8807180028928343063 ) ) ;
#34111=CARTESIAN_POINT ( 'NONE',  ( -129.5562042904834072, -24.64898659630529920, 1.056161002820838579 ) ) ;
#34112=ORIENTED_EDGE ( 'NONE', *, *, #5215, .F. ) ;
#34115=CARTESIAN_POINT ( 'NONE',  ( -87.62287095715004170, -24.33832256526968862, 0.1851278514119903129 ) ) ;
#34118=CARTESIAN_POINT ( 'NONE',  ( 9.480266252741309074, -18.97159823121752709, -1.500000000000002220 ) ) ;
#34119=EDGE_CURVE ( 'NONE', #88641, #75066, #37062, .T. ) ;
#34120=VERTEX_POINT ( 'NONE', #49135 ) ;
#34121=CARTESIAN_POINT ( 'NONE',  ( -88.62863264088480264, -24.34968618360934656, 0.1864209137778829184 ) ) ;
#34122=CARTESIAN_POINT ( 'NONE',  ( 9.711643268838683341, -19.58466107313252635, 11.49999999999998934 ) ) ;
#34123=CARTESIAN_POINT ( 'NONE',  ( -52.59912202816710902, -23.96169478059712787, 10.65365249895718591 ) ) ;
#34124=CARTESIAN_POINT ( 'NONE',  ( -41.35158263814751933, -25.28892524829919708, 3.766620786843653867 ) ) ;
#34125=CARTESIAN_POINT ( 'NONE',  ( -49.52287095715006870, -24.35013146730202749, 9.818937971375111928 ) ) ;
#34126=CARTESIAN_POINT ( 'NONE',  ( 1.740910633133015972, 21.82039641801506846, -1.500000000000002220 ) ) ;
#34127=CARTESIAN_POINT ( 'NONE',  ( -109.5228709571500616, -23.48786465467242479, 11.44779295918253936 ) ) ;
#34130=CARTESIAN_POINT ( 'NONE',  ( -49.18705952543585624, -25.26337497496688300, 7.035471253413802195 ) ) ;
#34133=ORIENTED_EDGE ( 'NONE', *, *, #7869, .F. ) ;
#34139=VECTOR ( 'NONE', #30470, 1000.000000000000114 ) ;
#34140=CARTESIAN_POINT ( 'NONE',  ( -31.24388727629348494, -25.27868065289452559, 3.907572214828554991 ) ) ;
#34141=CARTESIAN_POINT ( 'NONE',  ( -10.85727797829764185, 18.24708236899833835, -1.500000000000002220 ) ) ;
#34143=CARTESIAN_POINT ( 'NONE',  ( -102.6228709571500559, -23.47593901973091235, -1.443836447539001089 ) ) ;
#34144=B_SPLINE_CURVE_WITH_KNOTS ( 'NONE', 3,
 ( #94660, #18037, #71335, #57619, #1824, #95166 ),
 .UNSPECIFIED., .F., .F.,
 ( 4, 2, 4 ),
 ( 6.384118694778946581E-06, 0.001386860460836456194, 0.002767336802978133219 ),
 .UNSPECIFIED. ) ;
#34146=CARTESIAN_POINT ( 'NONE',  ( -129.5228709571501042, -24.51283580621366553, 0.6167428607019809217 ) ) ;
#34147=AXIS2_PLACEMENT_3D ( 'NONE', #25278, #47132, #62356 ) ;
#34148=CARTESIAN_POINT ( 'NONE',  ( 6.036767712469883307, 18.47306877840545170, -1.500000000000002220 ) ) ;
#34149=CARTESIAN_POINT ( 'NONE',  ( -45.52251770710876855, -25.00158670708910336, 2.256160236439225031 ) ) ;
#34151=CARTESIAN_POINT ( 'NONE',  ( 17.47348308817029405, 8.859467055162037141, 11.49999999999999645 ) ) ;
#34153=DIRECTION ( 'NONE',  ( 0.000000000000000000, -0.9999999999976377785, -2.173523156925979975E-06 ) ) ;
#34154=VERTEX_POINT ( 'NONE', #18655 ) ;
#34155=CARTESIAN_POINT ( 'NONE',  ( -97.62287095715008434, -23.94994826722515668, -0.6494450866351703100 ) ) ;
#34156=CARTESIAN_POINT ( 'NONE',  ( -89.55152734856552854, -24.15543982623907837, -0.2315651400026483009 ) ) ;
#34158=CARTESIAN_POINT ( 'NONE',  ( -80.64549629918748508, -25.03156060304832664, 7.560538530590703132 ) ) ;
#34159=CARTESIAN_POINT ( 'NONE',  ( 19.63295818312489871, -1.572306604260808260, 11.49999999999998934 ) ) ;
#34160=EDGE_LOOP ( 'NONE', ( #27545, #12464, #80556, #76669 ) ) ;
#34161=CARTESIAN_POINT ( 'NONE',  ( -121.6228709571500417, -24.64898659630368627, 1.056161002820833028 ) ) ;
#34162=PLANE ( 'NONE',  #80355 ) ;
#34164=ORIENTED_EDGE ( 'NONE', *, *, #3725, .T. ) ;
#34165=CARTESIAN_POINT ( 'NONE',  ( -125.5228709571500048, -24.83620972994592435, 8.398175272781372769 ) ) ;
#34167=CARTESIAN_POINT ( 'NONE',  ( -108.9623037622677941, -25.26366506051257588, 3.989953612098970481 ) ) ;
#34168=CARTESIAN_POINT ( 'NONE',  ( -76.52287095715007581, -24.65952944569304606, 1.056160979905698794 ) ) ;
#34169=CARTESIAN_POINT ( 'NONE',  ( -119.5228709571500758, -24.64898659630368627, 1.056161002820833028 ) ) ;
#34170=CARTESIAN_POINT ( 'NONE',  ( -69.51029376924685721, -25.31201676907213027, 5.710789725594461075 ) ) ;
#34171=PLANE ( 'NONE',  #91542 ) ;
#34172=CARTESIAN_POINT ( 'NONE',  ( 18.23660095519748481, -8.086948576924280374, 11.49999999999998934 ) ) ;
#34173=CARTESIAN_POINT ( 'NONE',  ( -100.6945227148491426, -25.19910511675319853, 3.322861593611079467 ) ) ;
#34174=CARTESIAN_POINT ( 'NONE',  ( -19.77004505525285083, 2.005399880840008642, -1.500000000000002220 ) ) ;
#34175=VERTEX_POINT ( 'NONE', #88683 ) ;
#34176=CARTESIAN_POINT ( 'NONE',  ( -84.62287095715005592, -29.50250786944525672, 11.44777988621623521 ) ) ;
#34177=B_SPLINE_CURVE_WITH_KNOTS ( 'NONE', 3,
 ( #62194, #68799, #30221, #70798 ),
 .UNSPECIFIED., .F., .F.,
 ( 4, 4 ),
 ( 0.1105789617298616606, 0.1195853930019770833 ),
 .UNSPECIFIED. ) ;
#34178=CARTESIAN_POINT ( 'NONE',  ( -51.22247509701755774, -25.17612187086679043, 6.839882705316316702 ) ) ;
#34180=CARTESIAN_POINT ( 'NONE',  ( -80.49409576116666187, -24.92592662359561118, 8.075495903017996469 ) ) ;
#34181=CARTESIAN_POINT ( 'NONE',  ( 19.72710162658169608, 6.580912942549038469, 11.49999999999999645 ) ) ;
#34185=CARTESIAN_POINT ( 'NONE',  ( 22.22072617242880455, -5.352622178732230118, 11.49999999999999645 ) ) ;
#34186=EDGE_LOOP ( 'NONE', ( #90865, #32373, #54796, #3096 ) ) ;
#34188=CARTESIAN_POINT ( 'NONE',  ( -74.62287095715005592, -29.50247984919015209, -1.443849546365055359 ) ) ;
#34189=CARTESIAN_POINT ( 'NONE',  ( -50.40445135320379677, -29.50249842297920466, 7.101626040072651413 ) ) ;
#34191=CARTESIAN_POINT ( 'NONE',  ( 19.26017855675105750, 6.235128648364509196, -1.500000000000002220 ) ) ;
#34192=CARTESIAN_POINT ( 'NONE',  ( -90.52287095715006160, -23.47596703998600631, 11.44779298504228393 ) ) ;
#34193=CARTESIAN_POINT ( 'NONE',  ( -129.6228709571500701, -24.50216790748205398, 0.6166512839542656055 ) ) ;
#34196=CARTESIAN_POINT ( 'NONE',  ( -84.52287095715006160, -24.64898659630528854, 1.056161002820826145 ) ) ;
#34197=EDGE_CURVE ( 'NONE', #17879, #33339, #63694, .T. ) ;
#34198=ORIENTED_EDGE ( 'NONE', *, *, #100288, .T. ) ;
#34200=CARTESIAN_POINT ( 'NONE',  ( -77.52287095715010423, -23.47593901973090524, -1.443836447538997092 ) ) ;
#34202=CARTESIAN_POINT ( 'NONE',  ( 15.90762396150235958, 12.10710967819287198, -1.500000000000002220 ) ) ;
#34203=CARTESIAN_POINT ( 'NONE',  ( 20.69369447470243628, -3.267675865747468489, 11.49999999999999645 ) ) ;
#34205=EDGE_CURVE ( 'NONE', #87248, #15603, #40673, .T. ) ;
#34208=CARTESIAN_POINT ( 'NONE',  ( 2.156995527713877259, 21.93451973775924557, 11.49999999999998934 ) ) ;
#34209=CARTESIAN_POINT ( 'NONE',  ( -39.71177198204633640, -25.31589273396069473, 4.822383007266354049 ) ) ;
#34211=CARTESIAN_POINT ( 'NONE',  ( -60.52287095715007581, -24.91544648472619983, 1.928969306349231250 ) ) ;
#34212=CARTESIAN_POINT ( 'NONE',  ( -117.5228709571500758, -23.47593901973090524, -1.443836447538996204 ) ) ;
#34213=CARTESIAN_POINT ( 'NONE',  ( -72.59671298878585333, -23.96119346886880663, -0.6495511937832119109 ) ) ;
#34214=DIRECTION ( 'NONE',  ( -3.773278334453079618E-23, 0.9999999999976377785, 2.173523156925979975E-06 ) ) ;
#34218=CARTESIAN_POINT ( 'NONE',  ( -36.52287095715006870, -29.50250243563736774, 8.947779886222148704 ) ) ;
#34219=CARTESIAN_POINT ( 'NONE',  ( -129.5228709571500758, -23.48786465467242479, 11.44779295918253581 ) ) ;
#34220=CARTESIAN_POINT ( 'NONE',  ( 10.70087849588422380, -17.49211976490306597, -1.500000000000002220 ) ) ;
#34222=ORIENTED_EDGE ( 'NONE', *, *, #72614, .T. ) ;
#34223=CARTESIAN_POINT ( 'NONE',  ( -39.52287095715006870, -24.65952944569304606, 1.056160979905691910 ) ) ;
#34225=CARTESIAN_POINT ( 'NONE',  ( -41.52287095715009002, -24.33927499327854349, 9.819080762295811837 ) ) ;
#34226=CARTESIAN_POINT ( 'NONE',  ( 21.15698459081360383, -7.064864530413820454, -1.500000000000002220 ) ) ;
#34227=CARTESIAN_POINT ( 'NONE',  ( -0.1051616404667204685, -21.68859992388200908, -0.4716817114508830566 ) ) ;
#34229=EDGE_CURVE ( 'NONE', #56711, #11930, #73196, .T. ) ;
#34230=ORIENTED_EDGE ( 'NONE', *, *, #36774, .F. ) ;
#34231=CARTESIAN_POINT ( 'NONE',  ( -42.62287095715004170, -23.94994826722515313, -0.6494450866351717533 ) ) ;
#34232=CARTESIAN_POINT ( 'NONE',  ( -51.68090471422387111, -25.27854796960392036, 4.190565742094029211 ) ) ;
#34233=CARTESIAN_POINT ( 'NONE',  ( -19.30504728598367237, -7.930543132070424051, -1.500000000000002220 ) ) ;
#34234=VERTEX_POINT ( 'NONE', #18165 ) ;
#34235=CARTESIAN_POINT ( 'NONE',  ( -39.04646076302208257, -25.27410141243213459, 4.123264079031926599 ) ) ;
#34239=CARTESIAN_POINT ( 'NONE',  ( -33.58953762381672448, -23.47593901973091235, -1.443836447539013301 ) ) ;
#34240=CARTESIAN_POINT ( 'NONE',  ( 18.71565868802652588, -9.641079743366450572, -1.500000000000002220 ) ) ;
#34242=CARTESIAN_POINT ( 'NONE',  ( -37.52287095715006870, -23.47596703998600631, 11.44779298504229281 ) ) ;
#34244=CARTESIAN_POINT ( 'NONE',  ( -105.5895376238167103, -25.00182538069145721, 7.747789668545099317 ) ) ;
#34245=CARTESIAN_POINT ( 'NONE',  ( -101.5316874056614012, -25.25419461862107795, 7.138212572458112248 ) ) ;
#34246=CARTESIAN_POINT ( 'NONE',  ( -84.52287095715006160, -23.47593901973090524, -1.443836447538996648 ) ) ;
#34247=CARTESIAN_POINT ( 'NONE',  ( 16.47784684176308545, -14.13017478139203220, -1.500000000000002220 ) ) ;
#34248=CARTESIAN_POINT ( 'NONE',  ( -81.29833273411215089, -25.12224311376198926, 6.730504961598555269 ) ) ;
#34249=CARTESIAN_POINT ( 'NONE',  ( 14.63995501510512653, -16.76770752772931772, 11.49999999999999645 ) ) ;
#34250=ORIENTED_EDGE ( 'NONE', *, *, #36952, .T. ) ;
#34251=CARTESIAN_POINT ( 'NONE',  ( -51.52764846858840997, -25.24728938674537559, 6.187572788865870699 ) ) ;
#34253=CARTESIAN_POINT ( 'NONE',  ( -69.58953762381672448, -23.48786465467241058, 11.44779295918254824 ) ) ;
#34254=EDGE_CURVE ( 'NONE', #27148, #5489, #64874, .T. ) ;
#34255=ORIENTED_EDGE ( 'NONE', *, *, #71475, .F. ) ;
#34258=ORIENTED_EDGE ( 'NONE', *, *, #75795, .F. ) ;
#34259=ORIENTED_EDGE ( 'NONE', *, *, #173, .F. ) ;
#34260=B_SPLINE_CURVE_WITH_KNOTS ( 'NONE', 3,
 ( #58065, #89491, #88999, #20464 ),
 .UNSPECIFIED., .F., .F.,
 ( 4, 4 ),
 ( 0.000000000000000000, 9.999999999998897304E-05 ),
 .UNSPECIFIED. ) ;
#34264=PLANE ( 'NONE',  #66444 ) ;
#34266=ORIENTED_EDGE ( 'NONE', *, *, #35767, .T. ) ;
#34268=CARTESIAN_POINT ( 'NONE',  ( -130.5728709571500588, -23.56000036390797092, -1.497999999999531040 ) ) ;
#34269=( BOUNDED_SURFACE ( )  B_SPLINE_SURFACE ( 3, 1, ( 
 ( #86977, #77355 ),
 ( #2262, #63164 ),
 ( #31699, #9857 ),
 ( #69768, #16458 ) ),
 .UNSPECIFIED., .F., .F., .T. ) 
 B_SPLINE_SURFACE_WITH_KNOTS ( ( 4, 4 ),
 ( 2, 2 ),
 ( 0.000000000000000000, 1.000000000000000000 ),
 ( 0.000000000000000000, 1.000000000000000000 ),
 .UNSPECIFIED. ) 
 GEOMETRIC_REPRESENTATION_ITEM ( )  RATIONAL_B_SPLINE_SURFACE ( (
 ( 1.000000000000000000, 1.000000000000000000),
 ( 0.3333333333333321491, 0.3333333333333321491),
 ( 0.3333333333333321491, 0.3333333333333321491),
 ( 1.000000000000000000, 1.000000000000000000) ) ) 
 REPRESENTATION_ITEM ( '' )  SURFACE ( )  );
#34270=CARTESIAN_POINT ( 'NONE',  ( 11.54466316424315231, -19.26756404802103972, -1.500000000000002220 ) ) ;
#34272=CARTESIAN_POINT ( 'NONE',  ( -112.5188917146773093, -23.96169478059713498, 10.65365249895717170 ) ) ;
#34273=CARTESIAN_POINT ( 'NONE',  ( -88.52287095715006160, -29.50250786944525672, 11.44777988621623344 ) ) ;
#34275=CARTESIAN_POINT ( 'NONE',  ( -49.22287095715007865, -23.47593901973090169, -1.443836447538997980 ) ) ;
#34276=CARTESIAN_POINT ( 'NONE',  ( -30.57310316700385400, -25.30558673197060671, 5.002395802403323266 ) ) ;
#34278=CARTESIAN_POINT ( 'NONE',  ( 12.01011565470214393, -15.49198969801113890, 11.49999999999998934 ) ) ;
#34282=CARTESIAN_POINT ( 'NONE',  ( -14.35963886870962192, 16.04489112172382903, 11.49999999999998934 ) ) ;
#34284=CARTESIAN_POINT ( 'NONE',  ( -80.64958649024407578, -25.30394762175274437, 4.980655888648957585 ) ) ;
#34286=CARTESIAN_POINT ( 'NONE',  ( -72.62287095715005592, -23.48783264082478084, -1.443836473390067265 ) ) ;
#34287=CARTESIAN_POINT ( 'NONE',  ( -21.13427563780003382, 8.902639844219676135, -1.500000000000002220 ) ) ;
#34289=CARTESIAN_POINT ( 'NONE',  ( -93.62287095715002749, -24.51283580621365132, 0.6167428607019797004 ) ) ;
#34290=CARTESIAN_POINT ( 'NONE',  ( -49.50098155592819893, -24.15543982623906771, -0.2315651400026657036 ) ) ;
#34291=CARTESIAN_POINT ( 'NONE',  ( -7.287290609967129740, 18.71191762695291771, 11.49999999999999645 ) ) ;
#34292=FACE_OUTER_BOUND ( 'NONE', #89425, .T. ) ;
#34294=CARTESIAN_POINT ( 'NONE',  ( -89.62287095715004170, -29.50250786944525672, 11.44777988621623344 ) ) ;
#34297=CARTESIAN_POINT ( 'NONE',  ( -7.754168067426306266, 18.25094163199162622, 11.49999999999998934 ) ) ;
#34299=CARTESIAN_POINT ( 'NONE',  ( -2.355416116969162754, -19.56741566493107598, -1.500000000000002220 ) ) ;
#34302=PLANE ( 'NONE',  #80777 ) ;
#34304=CARTESIAN_POINT ( 'NONE',  ( 9.149160795417088821, -18.46424698110740437, 11.49999999999999645 ) ) ;
#34306=CARTESIAN_POINT ( 'NONE',  ( -22.58250372949163420, -2.080990182559540269, 11.49999999999999645 ) ) ;
#34308=ORIENTED_EDGE ( 'NONE', *, *, #60434, .F. ) ;
#34309=CARTESIAN_POINT ( 'NONE',  ( -69.50411869601543913, -25.25639515137636337, 6.704350647680200836 ) ) ;
#34310=CARTESIAN_POINT ( 'NONE',  ( -50.90364520198352238, -25.30916279181417394, 4.601666023064476363 ) ) ;
#34311=EDGE_CURVE ( 'NONE', #88227, #3088, #94930, .T. ) ;
#34313=CARTESIAN_POINT ( 'NONE',  ( -26.72222193076970953, -24.61460054499585226, 7.978875576793555524 ) ) ;
#34316=EDGE_CURVE ( 'NONE', #3681, #77123, #61160, .T. ) ;
#34317=ORIENTED_EDGE ( 'NONE', *, *, #93177, .T. ) ;
#34318=CARTESIAN_POINT ( 'NONE',  ( -99.56054792670708764, -25.17640016615229470, 6.770854614618325051 ) ) ;
#34319=CARTESIAN_POINT ( 'NONE',  ( 13.94817355369617751, 18.09530419158152625, 11.49999999999998934 ) ) ;
#34320=CARTESIAN_POINT ( 'NONE',  ( -98.62287095715005592, -24.64965695001469115, 8.947790433994178727 ) ) ;
#34321=CARTESIAN_POINT ( 'NONE',  ( -113.5508033655503510, -24.66019654487200086, 8.947790411086106843 ) ) ;
#34322=CARTESIAN_POINT ( 'NONE',  ( -82.50021946911930115, -24.66019654487199730, 8.947790411086122830 ) ) ;
#34323=CARTESIAN_POINT ( 'NONE',  ( -22.33494257564923302, 2.542849975942539587, 11.49999999999999645 ) ) ;
#34324=ORIENTED_EDGE ( 'NONE', *, *, #6477, .F. ) ;
#34326=VECTOR ( 'NONE', #48527, 1000.000000000000114 ) ;
#34327=CARTESIAN_POINT ( 'NONE',  ( 16.22650188657148362, -14.79325693486936188, 11.49999999999998934 ) ) ;
#34328=CARTESIAN_POINT ( 'NONE',  ( -125.2170317540820861, -25.33540041250694230, 3.690481496468096090 ) ) ;
#34329=B_SPLINE_CURVE_WITH_KNOTS ( 'NONE', 3,
 ( #50700, #4532, #13118, #58812, #42103, #51200 ),
 .UNSPECIFIED., .F., .F.,
 ( 4, 2, 4 ),
 ( 6.384118695309162101E-06, 0.001386860460836723992, 0.002767336802978138856 ),
 .UNSPECIFIED. ) ;
#34330=CARTESIAN_POINT ( 'NONE',  ( -44.55312310627501660, -23.96169478059713143, 10.65365249895718414 ) ) ;
#34331=CARTESIAN_POINT ( 'NONE',  ( -118.6228709571500701, -23.48783264082478794, -1.443836473390058384 ) ) ;
#34335=DIRECTION ( 'NONE',  ( -3.773278334444167608E-23, 1.000000000000000000, 0.000000000000000000 ) ) ;
#34336=VERTEX_POINT ( 'NONE', #28146 ) ;
#34337=CARTESIAN_POINT ( 'NONE',  ( -88.52287095715006160, -23.94994826722564696, -0.6494450866342719175 ) ) ;
#34338=CARTESIAN_POINT ( 'NONE',  ( 6.429960413904108663, -19.47341730443774921, 11.49999999999998934 ) ) ;
#34343=CARTESIAN_POINT ( 'NONE',  ( 21.75596283627254479, -7.788036635067100200, -1.500000000000002220 ) ) ;
#34344=DIRECTION ( 'NONE',  ( -3.773278334453079030E-23, 0.9999999999976377785, 2.173523156925979128E-06 ) ) ;
#34345=CARTESIAN_POINT ( 'NONE',  ( 20.27773211485958527, -1.686570798567030183, -1.500000000000002220 ) ) ;
#34346=ORIENTED_EDGE ( 'NONE', *, *, #76721, .T. ) ;
#34348=CARTESIAN_POINT ( 'NONE',  ( -29.61081068843649433, -23.65861429716871100, 11.05961561336856569 ) ) ;
#34350=CARTESIAN_POINT ( 'NONE',  ( -105.5468799023555562, -24.92564183028979130, 1.928384488918251316 ) ) ;
#34351=FACE_OUTER_BOUND ( 'NONE', #86123, .T. ) ;
#34357=CARTESIAN_POINT ( 'NONE',  ( 0.4431998670617953717, 20.78131286043265646, -1.500000000000002220 ) ) ;
#34358=ORIENTED_EDGE ( 'NONE', *, *, #93985, .F. ) ;
#34359=CARTESIAN_POINT ( 'NONE',  ( -39.44891728460616775, -25.28243733276015348, 4.250048832811843091 ) ) ;
#34360=ORIENTED_EDGE ( 'NONE', *, *, #72627, .T. ) ;
#34362=DIRECTION ( 'NONE',  ( -3.773278334453079030E-23, 0.9999999999976377785, 2.173523156925978705E-06 ) ) ;
#34365=CARTESIAN_POINT ( 'NONE',  ( -29.62287095715004881, -24.57333416927490433, 1.056161302446588124 ) ) ;
#34367=CARTESIAN_POINT ( 'NONE',  ( -70.97512524164069703, -25.24515085444608431, 5.512439509005878868 ) ) ;
#34368=CARTESIAN_POINT ( 'NONE',  ( -19.90388773112789167, 9.559999800501117306, 11.49999999999999645 ) ) ;
#34370=CARTESIAN_POINT ( 'NONE',  ( -47.62287095715004881, -23.48786465467240703, 11.44779295918255180 ) ) ;
#34371=CARTESIAN_POINT ( 'NONE',  ( 15.43685675143394498, -16.52047792065556564, 11.49999999999998934 ) ) ;
#34372=B_SPLINE_CURVE_WITH_KNOTS ( 'NONE', 3,
 ( #54498, #47389, #79323, #9817, #40767, #85433, #8822, #71728 ),
 .UNSPECIFIED., .F., .F.,
 ( 4, 2, 2, 4 ),
 ( -0.001240355328176878311, -0.0002398155169399626176, 0.0007607242942969530755, 0.002761803916770787931 ),
 .UNSPECIFIED. ) ;
#34376=ORIENTED_EDGE ( 'NONE', *, *, #77896, .F. ) ;
#34378=EDGE_CURVE ( 'NONE', #294, #88628, #40486, .T. ) ;
#34382=CARTESIAN_POINT ( 'NONE',  ( -19.98373207111551508, 7.008865001458166155, -1.500000000000002220 ) ) ;
#34384=CARTESIAN_POINT ( 'NONE',  ( -125.6228709571500559, -23.47593901973091235, -1.443836447538995760 ) ) ;
#34386=CARTESIAN_POINT ( 'NONE',  ( 7.688942331755139747, 20.87172568467934752, -1.500000000000002220 ) ) ;
#34387=CARTESIAN_POINT ( 'NONE',  ( -114.5158209565278469, -24.51314013834316086, 0.6176544820404251679 ) ) ;
#34391=CARTESIAN_POINT ( 'NONE',  ( -36.51285728403535558, -23.73791477778911130, 11.05961554403171121 ) ) ;
#34393=CARTESIAN_POINT ( 'NONE',  ( -10.28394983263804185, -16.58134856480417341, 11.49999999999998934 ) ) ;
#34395=CARTESIAN_POINT ( 'NONE',  ( 6.977786103627443559, 20.27319509581574408, -1.500000000000002220 ) ) ;
#34396=CARTESIAN_POINT ( 'NONE',  ( -26.47871760004291630, -24.92774763277149574, 2.074684386906315847 ) ) ;
#34397=AXIS2_PLACEMENT_3D ( 'NONE', #98538, #28535, #51389 ) ;
#34398=LINE ( 'NONE', #2963, #35735 ) ;
#34399=CARTESIAN_POINT ( 'NONE',  ( -77.54621141149542041, -24.34968618360934300, 0.1864209137778811143 ) ) ;
#34400=CARTESIAN_POINT ( 'NONE',  ( -13.73562189146022661, -18.16285900770654393, -1.500000000000002220 ) ) ;
#34401=B_SPLINE_CURVE_WITH_KNOTS ( 'NONE', 3,
 ( #84645, #46097, #77024, #98865 ),
 .UNSPECIFIED., .F., .F.,
 ( 4, 4 ),
 ( 1.387778780781445676E-17, 0.0001000000000000028508 ),
 .UNSPECIFIED. ) ;
#34403=CARTESIAN_POINT ( 'NONE',  ( -102.5909830230292386, -24.15543982623908192, -0.2315651400026459694 ) ) ;
#34405=CARTESIAN_POINT ( 'NONE',  ( -10.29545327866581950, 17.06371652956568852, 11.49999999999999645 ) ) ;
#34406=PLANE ( 'NONE',  #77787 ) ;
#34407=B_SPLINE_CURVE_WITH_KNOTS ( 'NONE', 3,
 ( #36507, #5063, #75061, #5561 ),
 .UNSPECIFIED., .F., .F.,
 ( 4, 4 ),
 ( 0.7903502942768684258, 0.7993567255489840706 ),
 .UNSPECIFIED. ) ;
#34408=CARTESIAN_POINT ( 'NONE',  ( -39.62372017418730508, -24.66019654487198665, 8.947790411086131712 ) ) ;
#34409=CARTESIAN_POINT ( 'NONE',  ( -48.54706234259929687, -24.15543982623907482, -0.2315651400026527418 ) ) ;
#34412=CARTESIAN_POINT ( 'NONE',  ( -32.40343208386849483, -25.31558585043574183, 4.997857581739419075 ) ) ;
#34413=CARTESIAN_POINT ( 'NONE',  ( -1.268225406894735396, -21.67698866206750097, 11.49999999999998934 ) ) ;
#34414=CARTESIAN_POINT ( 'NONE',  ( -51.84991333203042529, -25.20452363795868678, 6.645056544736056559 ) ) ;
#34415=CARTESIAN_POINT ( 'NONE',  ( -9.112395119859147741, -17.30902560603237106, -1.500000000000002220 ) ) ;
#34421=FACE_OUTER_BOUND ( 'NONE', #34186, .T. ) ;
#34422=CARTESIAN_POINT ( 'NONE',  ( -2.750569593922542300, -20.27526743851804625, 11.49999999999999645 ) ) ;
#34423=LINE ( 'NONE', #65403, #27815 ) ;
#34424=CARTESIAN_POINT ( 'NONE',  ( -89.52287095715006160, -23.47593901973090169, -1.443836447538996426 ) ) ;
#34425=ORIENTED_EDGE ( 'NONE', *, *, #57170, .F. ) ;
#34429=DIRECTION ( 'NONE',  ( -1.000000000000000000, -3.773278334444167608E-23, -8.201307833595939069E-29 ) ) ;
#34430=AXIS2_PLACEMENT_3D ( 'NONE', #82534, #89656, #12025 ) ;
#34431=CARTESIAN_POINT ( 'NONE',  ( -109.5183339203764348, -23.96119346886880663, -0.6495511937832053606 ) ) ;
#34432=EDGE_CURVE ( 'NONE', #86774, #71695, #55032, .T. ) ;
#34433=ORIENTED_EDGE ( 'NONE', *, *, #93067, .T. ) ;
#34434=LINE ( 'NONE', #65414, #75499 ) ;
#34435=ADVANCED_FACE ( 'NONE', ( #89541 ), #34264, .F. ) ;
#34436=CARTESIAN_POINT ( 'NONE',  ( 22.25235761598246143, -5.642936543268669780, 11.49999999999999645 ) ) ;
#34437=CARTESIAN_POINT ( 'NONE',  ( 7.803535043518188274, -21.38454823780343617, -1.500000000000002220 ) ) ;
#34439=B_SPLINE_SURFACE_WITH_KNOTS ( 'NONE', 3, 3, ( 
 ( #16560, #47534, #76957, #78458 ),
 ( #63778, #70363, #1856, #39907 ),
 ( #92685, #31293, #17068, #85578 ),
 ( #56154, #16060, #47033, #848 ),
 ( #7451, #31803, #46527, #38910 ),
 ( #62773, #70873, #94186, #32297 ),
 ( #69865, #1363, #346, #24673 ),
 ( #48034, #9460, #94695, #38408 ),
 ( #40418, #25178, #100280, #30800 ),
 ( #61765, #18073, #58639, #88595 ) ),
 .UNSPECIFIED., .F., .F., .F.,
 ( 4, 3, 3, 4 ),
 ( 4, 4 ),
 ( 0.0004766839783823869237, 0.1491231665100173909, 0.2234464077758348821, 0.2977696490416523734 ),
 ( 0.09950601477590118038, 0.1005780351604402129 ),
 .UNSPECIFIED. ) ;
#34440=EDGE_CURVE ( 'NONE', #96725, #7991, #97449, .T. ) ;
#34442=CARTESIAN_POINT ( 'NONE',  ( -81.52287095715006160, -24.50321055353805377, 9.387540953477525818 ) ) ;
#34443=CARTESIAN_POINT ( 'NONE',  ( -78.58953762381671027, -23.48786465467241413, 11.44779295918254469 ) ) ;
#34444=ADVANCED_FACE ( 'NONE', ( #21014 ), #22499, .T. ) ;
#34445=CARTESIAN_POINT ( 'NONE',  ( -54.58953762381672448, -23.48786465467240347, 11.44779295918255180 ) ) ;
#34446=CARTESIAN_POINT ( 'NONE',  ( 8.256513476402210117, 20.27555108428041208, 11.49999999999998934 ) ) ;
#34447=CARTESIAN_POINT ( 'NONE',  ( -69.50159385232926468, -24.35071581493542681, 9.817618358456032368 ) ) ;
#34449=CARTESIAN_POINT ( 'NONE',  ( -49.74369414166533687, -25.31543073408252909, 4.940877929217667663 ) ) ;
#34450=CARTESIAN_POINT ( 'NONE',  ( -71.70422574834498164, -25.25838781600607419, 6.074309804579013594 ) ) ;
#34452=ORIENTED_EDGE ( 'NONE', *, *, #22255, .T. ) ;
#34453=CARTESIAN_POINT ( 'NONE',  ( 5.143668500415711442, -19.74887971880038151, -1.500000000000002220 ) ) ;
#34455=ORIENTED_EDGE ( 'NONE', *, *, #94827, .F. ) ;
#34456=ORIENTED_EDGE ( 'NONE', *, *, #71690, .F. ) ;
#34457=ADVANCED_FACE ( 'NONE', ( #98134 ), #70297, .T. ) ;
#34458=CARTESIAN_POINT ( 'NONE',  ( -14.43837761634077310, -17.93274050997184332, -1.500000000000002220 ) ) ;
#34460=CARTESIAN_POINT ( 'NONE',  ( -3.510519812331947875, -19.85243952969433323, -1.500000000000002220 ) ) ;
#34464=CARTESIAN_POINT ( 'NONE',  ( -95.54445644477492294, -24.83618233451450408, 1.606449574219538157 ) ) ;
#34466=CARTESIAN_POINT ( 'NONE',  ( 18.61059577090848549, -10.47110149595715711, 11.49999999999999645 ) ) ;
#34468=CARTESIAN_POINT ( 'NONE',  ( -55.52287095715010423, -24.14321612903117398, -0.2833117244521657918 ) ) ;
#34471=CARTESIAN_POINT ( 'NONE',  ( 18.30470771955606679, 12.64531542519679697, 11.49999999999998934 ) ) ;
#34472=CARTESIAN_POINT ( 'NONE',  ( -19.97286373971314433, -5.326668811655218327, -1.500000000000002220 ) ) ;
#34473=ORIENTED_EDGE ( 'NONE', *, *, #64830, .F. ) ;
#34474=PLANE ( 'NONE',  #74543 ) ;
#34475=ORIENTED_EDGE ( 'NONE', *, *, #93866, .T. ) ;
#34479=CARTESIAN_POINT ( 'NONE',  ( -2.499008156623981236, -20.81284420272260860, -1.500000000000002220 ) ) ;
#34480=CARTESIAN_POINT ( 'NONE',  ( -3.281320334969873631, 21.64054093270537393, 11.49999999999999645 ) ) ;
#34481=EDGE_CURVE ( 'NONE', #58570, #58197, #97728, .T. ) ;
#34483=CARTESIAN_POINT ( 'NONE',  ( 21.70358988458699301, 5.938112137899119070, 11.49999999999998934 ) ) ;
#34484=CARTESIAN_POINT ( 'NONE',  ( 15.12549221760053086, 14.48511125727034177, 11.49999999999998934 ) ) ;
#34487=CARTESIAN_POINT ( 'NONE',  ( -57.62287095715003460, -24.50216790748097395, 0.6166512839513648148 ) ) ;
#34489=CARTESIAN_POINT ( 'NONE',  ( -70.55620429048339304, -23.47596703998600276, 11.44779298504227505 ) ) ;
#34493=ORIENTED_EDGE ( 'NONE', *, *, #4531, .T. ) ;
#34494=CARTESIAN_POINT ( 'NONE',  ( -99.29687923781919778, -25.12215468360345128, 6.149712483925878104 ) ) ;
#34495=VERTEX_POINT ( 'NONE', #98719 ) ;
#34496=CARTESIAN_POINT ( 'NONE',  ( 7.480126432006339421, -20.11416664461015458, -1.500000000000002220 ) ) ;
#34499=ORIENTED_EDGE ( 'NONE', *, *, #63095, .T. ) ;
#34501=CARTESIAN_POINT ( 'NONE',  ( -19.97109070424261645, 6.737033823242594366, -1.500000000000002220 ) ) ;
#34505=CARTESIAN_POINT ( 'NONE',  ( -80.61306835763387824, -25.29534349779240188, 4.525992644586477098 ) ) ;
#34506=CARTESIAN_POINT ( 'NONE',  ( -109.3584176993576591, -25.28950181196791647, 4.206202504803813191 ) ) ;
#34507=CARTESIAN_POINT ( 'NONE',  ( -5.561696574893697509, -21.35426480686918538, -1.500000000000002220 ) ) ;
#34509=VERTEX_POINT ( 'NONE', #51067 ) ;
#34510=CARTESIAN_POINT ( 'NONE',  ( -116.5534077701025240, -24.34968618360935366, 0.1864209137779019587 ) ) ;
#34511=ADVANCED_FACE ( 'NONE', ( #36837 ), #36335, .F. ) ;
#34512=CARTESIAN_POINT ( 'NONE',  ( -111.6228709571500417, -24.51387760970724727, 9.387446482453414731 ) ) ;
#34513=CARTESIAN_POINT ( 'NONE',  ( -60.48077622483229021, -25.00158670708910336, 2.256160236439220590 ) ) ;
#34514=CARTESIAN_POINT ( 'NONE',  ( -62.63182337673452338, -24.35071581493542325, 9.817618358456032368 ) ) ;
#34516=CARTESIAN_POINT ( 'NONE',  ( -127.5228709571499763, -23.48783264082477373, -1.443836473390082586 ) ) ;
#34517=CARTESIAN_POINT ( 'NONE',  ( -1.966620079519992181, -21.27258529651320274, 11.49999999999998934 ) ) ;
#34518=CARTESIAN_POINT ( 'NONE',  ( -70.66315859205543859, -25.31500238285650184, 4.882613580410660070 ) ) ;
#34519=CARTESIAN_POINT ( 'NONE',  ( -52.52287095715009713, -23.48783264083416356, -1.443836473375487151 ) ) ;
#34521=CARTESIAN_POINT ( 'NONE',  ( -47.62287095715004881, -29.50247984919015209, -1.443849546365058689 ) ) ;
#34522=PRODUCT_DEFINITION ( 'UNKNOWN', '', #78135, #13440 ) ;
#34523=CARTESIAN_POINT ( 'NONE',  ( 18.14931799402153345, 13.46472642042223633, -1.500000000000002220 ) ) ;
#34524=B_SPLINE_SURFACE_WITH_KNOTS ( 'NONE', 3, 3, ( 
 ( #66463, #54093, #23606, #14507 ),
 ( #54580, #62201, #85515, #38347 ),
 ( #37365, #44979, #75904, #68806 ),
 ( #283, #84020, #93124, #68308 ),
 ( #30737, #77394, #51209, #7894 ),
 ( #85014, #92627, #46969, #45482 ),
 ( #82151, #14004, #46464, #53596 ) ),
 .UNSPECIFIED., .F., .F., .F.,
 ( 4, 3, 4 ),
 ( 4, 4 ),
 ( 0.7945040050992241421, 0.8970133687736501216, 0.9995227324480759901 ),
 ( 0.3795904564402555748, 0.3807784251392243857 ),
 .UNSPECIFIED. ) ;
#34527=DIRECTION ( 'NONE',  ( 0.000000000000000000, 2.173523156925980399E-06, -0.9999999999976378895 ) ) ;
#34528=CARTESIAN_POINT ( 'NONE',  ( -113.6228709571500559, -29.50250786944525672, 11.44777988621622988 ) ) ;
#34529=CARTESIAN_POINT ( 'NONE',  ( -13.31955177964949755, -14.60123061082138385, 11.49999999999999645 ) ) ;
#34531=CARTESIAN_POINT ( 'NONE',  ( -67.63121645805480853, -24.34968618360933235, 0.1864209137778811143 ) ) ;
#34534=CARTESIAN_POINT ( 'NONE',  ( -110.5562042904834072, -23.47593901973091235, -1.443836447538999312 ) ) ;
#34536=CARTESIAN_POINT ( 'NONE',  ( -67.52287095715006160, -29.50247984919015209, -1.443849546365055359 ) ) ;
#34537=CARTESIAN_POINT ( 'NONE',  ( -21.34238180412542718, 3.497892552127677135, -1.500000000000002220 ) ) ;
#34538=CARTESIAN_POINT ( 'NONE',  ( -76.62287095715007013, -29.50250786944525672, 11.44777988621623521 ) ) ;
#34539=CARTESIAN_POINT ( 'NONE',  ( -59.62287095715004881, -23.47593901973091235, -1.443836447539007972 ) ) ;
#34540=DIRECTION ( 'NONE',  ( -3.773278334453079618E-23, 0.9999999999976377785, 2.173523156925979975E-06 ) ) ;
#34541=CARTESIAN_POINT ( 'NONE',  ( -81.88534077628074215, -25.24685308744633616, 6.293942982122114671 ) ) ;
#34542=CARTESIAN_POINT ( 'NONE',  ( 1.028332004353105233, 19.75660188889424518, -1.500000000000002220 ) ) ;
#34543=ORIENTED_EDGE ( 'NONE', *, *, #50284, .T. ) ;
#34544=VECTOR ( 'NONE', #2357, 1000.000000000000114 ) ;
#34545=CARTESIAN_POINT ( 'NONE',  ( 3.949161919925879172, -19.86910077469890723, 11.49999999999999645 ) ) ;
#34548=ORIENTED_EDGE ( 'NONE', *, *, #61193, .F. ) ;
#34553=DIRECTION ( 'NONE',  ( 1.000000000000000000, 3.773278334444167608E-23, 8.201307833595939069E-29 ) ) ;
#34554=CARTESIAN_POINT ( 'NONE',  ( -81.58953762381673869, -24.65952944569305316, 1.056160979905705011 ) ) ;
#34555=CARTESIAN_POINT ( 'NONE',  ( 0.1258803491696451060, 20.03332480481931199, -1.500000000000002220 ) ) ;
#34556=EDGE_CURVE ( 'NONE', #88644, #10751, #13482, .T. ) ;
#34557=CARTESIAN_POINT ( 'NONE',  ( -82.62287095715004170, -23.47596703998600631, 11.44779298504227860 ) ) ;
#34558=ORIENTED_EDGE ( 'NONE', *, *, #70736, .T. ) ;
#34559=B_SPLINE_CURVE_WITH_KNOTS ( 'NONE', 3,
 ( #69948, #17664, #46628, #86173 ),
 .UNSPECIFIED., .F., .F.,
 ( 4, 4 ),
 ( 0.000000000000000000, 9.999999999998206125E-05 ),
 .UNSPECIFIED. ) ;
#34560=B_SPLINE_CURVE_WITH_KNOTS ( 'NONE', 3,
 ( #78808, #93042, #70222, #23521 ),
 .UNSPECIFIED., .F., .F.,
 ( 4, 4 ),
 ( 0.000000000000000000, 1.000000000000000000 ),
 .UNSPECIFIED. ) ;
#34563=CARTESIAN_POINT ( 'NONE',  ( -32.62287095715004881, -24.35013146730203815, 9.818937971375115481 ) ) ;
#34564=EDGE_CURVE ( 'NONE', #90802, #1762, #65810, .T. ) ;
#34565=DIRECTION ( 'NONE',  ( 1.000000000000000000, 3.773278334444167608E-23, 8.201307833595939069E-29 ) ) ;
#34566=CARTESIAN_POINT ( 'NONE',  ( -84.62287095715005592, -29.50248528299804818, 1.056150453629038477 ) ) ;
#34567=EDGE_CURVE ( 'NONE', #20207, #55313, #96200, .T. ) ;
#34568=CARTESIAN_POINT ( 'NONE',  ( -113.5228709571500332, -23.94994826722565406, -0.6494450866342719175 ) ) ;
#34569=CARTESIAN_POINT ( 'NONE',  ( -73.59228414436695687, -24.15543982623907127, -0.2315651400026654816 ) ) ;
#34573=ORIENTED_EDGE ( 'NONE', *, *, #70853, .F. ) ;
#34574=CARTESIAN_POINT ( 'NONE',  ( -16.58479117878708209, 11.75282063728064053, -1.500000000000002220 ) ) ;
#34576=ORIENTED_EDGE ( 'NONE', *, *, #84467, .T. ) ;
#34577=EDGE_CURVE ( 'NONE', #57603, #29911, #21094, .T. ) ;
#34578=CARTESIAN_POINT ( 'NONE',  ( -0.4961427919413599064, 22.93664481792237453, -1.500000000000002220 ) ) ;
#34581=CARTESIAN_POINT ( 'NONE',  ( -109.5228709571500616, -24.65952944569305316, 1.056160979905704123 ) ) ;
#34582=CARTESIAN_POINT ( 'NONE',  ( -50.16062266432883376, -25.12215416095027720, 7.085347845352387708 ) ) ;
#34584=CARTESIAN_POINT ( 'NONE',  ( -13.58512445790048417, 16.25115196636789250, 11.49999999999999645 ) ) ;
#34585=CARTESIAN_POINT ( 'NONE',  ( 2.574831182292884435, -22.01391258260016315, -1.500000000000002220 ) ) ;
#34586=CARTESIAN_POINT ( 'NONE',  ( 6.226698476505521995, -19.64469265145860177, -1.500000000000002220 ) ) ;
#34587=ORIENTED_EDGE ( 'NONE', *, *, #40380, .T. ) ;
#34588=CARTESIAN_POINT ( 'NONE',  ( -43.52287095715007581, -23.47593901973090169, -1.443836447538997092 ) ) ;
#34590=CARTESIAN_POINT ( 'NONE',  ( -54.49170867734796531, -24.51314013834315020, 0.6176544820404069602 ) ) ;
#34591=CARTESIAN_POINT ( 'NONE',  ( -126.6228709571500559, -23.96177878511310055, 10.65340807706329151 ) ) ;
#34593=EDGE_LOOP ( 'NONE', ( #90096, #16408, #18094, #24799 ) ) ;
#34594=B_SPLINE_CURVE_WITH_KNOTS ( 'NONE', 3,
 ( #29907, #75573, #67989, #22278, #52756, #83694 ),
 .UNSPECIFIED., .F., .F.,
 ( 4, 2, 4 ),
 ( 1.570755371633856203E-05, 0.001396183895866086886, 0.002776660238015835145 ),
 .UNSPECIFIED. ) ;
#34595=ORIENTED_EDGE ( 'NONE', *, *, #24452, .T. ) ;
#34597=DIRECTION ( 'NONE',  ( 0.000000000000000000, 2.173523156925980399E-06, -0.9999999999976378895 ) ) ;
#34598=DIRECTION ( 'NONE',  ( -3.773278334453079618E-23, 0.9999999999976377785, 2.173523156925979975E-06 ) ) ;
#34599=CARTESIAN_POINT ( 'NONE',  ( 4.358738815032396907, -20.29635662749097236, -1.500000000000002220 ) ) ;
#34600=CARTESIAN_POINT ( 'NONE',  ( -11.39883337241029793, 18.50525654427185884, 11.49999999999999645 ) ) ;
#34601=EDGE_LOOP ( 'NONE', ( #91959, #65470, #66562, #8743 ) ) ;
#34602=AXIS2_PLACEMENT_3D ( 'NONE', #20742, #15136, #5031 ) ;
#34603=CARTESIAN_POINT ( 'NONE',  ( -62.52287095715006160, -24.65952944569304606, 1.056160979905695463 ) ) ;
#34604=CARTESIAN_POINT ( 'NONE',  ( -96.62287095715004170, -24.65952944569304606, 1.056160979905703456 ) ) ;
#34605=CARTESIAN_POINT ( 'NONE',  ( 6.497064355747536268, 21.42967291005575348, 11.49999999999998934 ) ) ;
#34607=CARTESIAN_POINT ( 'NONE',  ( -57.62287095715004881, -23.47596703998600276, 11.44779298504227683 ) ) ;
#34611=DIRECTION ( 'NONE',  ( -3.773278334453079618E-23, 0.9999999999976377785, 2.173523156925979975E-06 ) ) ;
#34612=VECTOR ( 'NONE', #23410, 1000.000000000000114 ) ;
#34613=ORIENTED_EDGE ( 'NONE', *, *, #49674, .F. ) ;
#34614=EDGE_LOOP ( 'NONE', ( #70942, #76959, #49994, #81814 ) ) ;
#34615=CARTESIAN_POINT ( 'NONE',  ( -69.62287095715004170, -24.51387760970723662, 9.387446482453421837 ) ) ;
#34618=EDGE_CURVE ( 'NONE', #84065, #9013, #89622, .T. ) ;
#34619=CARTESIAN_POINT ( 'NONE',  ( 18.67678363807796416, 10.12720680154768971, -1.500000000000002220 ) ) ;
#34620=EDGE_LOOP ( 'NONE', ( #72141, #72657, #1800, #97232 ) ) ;
#34622=CARTESIAN_POINT ( 'NONE',  ( 21.83686239284238084, -0.8075297431944471471, 11.49999999999998934 ) ) ;
#34623=CARTESIAN_POINT ( 'NONE',  ( -103.5492830802958082, -24.51419770103155926, 9.386484678747176957 ) ) ;
#34624=CARTESIAN_POINT ( 'NONE',  ( -22.63693132222386950, 1.387278323242118416, -1.500000000000002220 ) ) ;
#34625=DIRECTION ( 'NONE',  ( -0.000000000000000000, 2.173523156925979552E-06, -0.9999999999976378895 ) ) ;
#34626=DIRECTION ( 'NONE',  ( 1.000000000000000000, 3.773278334444166432E-23, 8.201307841325785021E-29 ) ) ;
#34627=CARTESIAN_POINT ( 'NONE',  ( -17.40403014803320758, -13.24600170205644289, -1.500000000000002220 ) ) ;
#34629=EDGE_LOOP ( 'NONE', ( #51476, #1238, #23582, #1644 ) ) ;
#34630=CARTESIAN_POINT ( 'NONE',  ( -65.62287095715007013, -24.83602698348160942, 1.605859176311267511 ) ) ;
#34631=CARTESIAN_POINT ( 'NONE',  ( -126.5895376238167529, -24.65952944569305316, 1.056160979905704123 ) ) ;
#34635=LINE ( 'NONE', #74191, #49203 ) ;
#34636=FACE_BOUND ( 'NONE', #56210, .T. ) ;
#34637=CARTESIAN_POINT ( 'NONE',  ( 19.98919582620916913, -7.218065965386815996, -1.500000000000002220 ) ) ;
#34641=CARTESIAN_POINT ( 'NONE',  ( -85.58737842399442286, -24.63355581998386157, 0.9682620441943895484 ) ) ;
#34642=CARTESIAN_POINT ( 'NONE',  ( -68.63577655697397972, -24.15543982623907127, -0.2315651400026649820 ) ) ;
#34643=VECTOR ( 'NONE', #42654, 1000.000000000000114 ) ;
#34644=CARTESIAN_POINT ( 'NONE',  ( -117.6260431914922862, -24.15620529776629510, 10.23563542870659582 ) ) ;
#34646=CARTESIAN_POINT ( 'NONE',  ( 9.052818235119415746, 17.31195010612007223, 11.49999999999999645 ) ) ;
#34649=CARTESIAN_POINT ( 'NONE',  ( -29.81066147699621283, -25.24716167724356097, 5.128593285976438487 ) ) ;
#34652=ADVANCED_FACE ( 'NONE', ( #43458 ), #91110, .T. ) ;
#34653=CARTESIAN_POINT ( 'NONE',  ( -99.45104055277701605, -25.25095879578016422, 5.670438387523640600 ) ) ;
#34654=CARTESIAN_POINT ( 'NONE',  ( -80.52287095715006160, -23.47596703998600631, 11.44779298504228571 ) ) ;
#34656=CARTESIAN_POINT ( 'NONE',  ( 11.88433821776028942, -15.71472908967258242, -1.500000000000002220 ) ) ;
#34657=EDGE_CURVE ( 'NONE', #11314, #13213, #35834, .T. ) ;
#34662=ORIENTED_EDGE ( 'NONE', *, *, #54713, .F. ) ;
#34664=CARTESIAN_POINT ( 'NONE',  ( -123.6228709571500559, -29.50250243563736774, 8.947779886222134493 ) ) ;
#34665=CARTESIAN_POINT ( 'NONE',  ( -47.51396546215941186, -23.73766607897670866, -1.055555164236438692 ) ) ;
#34667=CARTESIAN_POINT ( 'NONE',  ( -79.91667645764968597, -25.33009845126374415, 4.495758016894969344 ) ) ;
#34669=CARTESIAN_POINT ( 'NONE',  ( -97.62287095715004170, -24.65952944569304606, 1.056160979905701236 ) ) ;
#34670=CARTESIAN_POINT ( 'NONE',  ( 12.75013301566243129, -15.34773647900153115, -1.500000000000002220 ) ) ;
#34673=CARTESIAN_POINT ( 'NONE',  ( -0.08316136044590859144, -21.97341083746030321, 10.06556358067885348 ) ) ;
#34674=CARTESIAN_POINT ( 'NONE',  ( 4.300141163375406528, 19.41444791797076874, -1.500000000000002220 ) ) ;
#34675=ORIENTED_EDGE ( 'NONE', *, *, #56232, .F. ) ;
#34679=CARTESIAN_POINT ( 'NONE',  ( 5.792680761630559338, -19.98616098212858105, 11.49999999999999645 ) ) ;
#34681=EDGE_CURVE ( 'NONE', #70270, #63070, #33284, .T. ) ;
#34683=CARTESIAN_POINT ( 'NONE',  ( 22.79674358141071977, 1.614764915196592598, 11.49999999999999645 ) ) ;
#34684=VERTEX_POINT ( 'NONE', #51567 ) ;
#34685=PLANE ( 'NONE',  #34919 ) ;
#34687=DIRECTION ( 'NONE',  ( -1.000000000000000000, -3.773278334444166432E-23, -8.201307841325785021E-29 ) ) ;
#34688=VERTEX_POINT ( 'NONE', #69779 ) ;
#34689=CARTESIAN_POINT ( 'NONE',  ( 6.697674113365701842, 19.09646837838083400, -1.500000000000002220 ) ) ;
#34698=CARTESIAN_POINT ( 'NONE',  ( 11.63622169266987783, 16.31392799894670631, -1.500000000000002220 ) ) ;
#34699=CARTESIAN_POINT ( 'NONE',  ( 16.43158684610488862, 13.14696595092960152, 11.49999999999999645 ) ) ;
#34701=CARTESIAN_POINT ( 'NONE',  ( -124.6228709571500133, -24.33927499327854704, 9.819080762295811837 ) ) ;
#34702=CARTESIAN_POINT ( 'NONE',  ( 11.67614657018352453, 18.69773523334854914, 11.49999999999998934 ) ) ;
#34704=FACE_OUTER_BOUND ( 'NONE', #78751, .T. ) ;
#34705=CARTESIAN_POINT ( 'NONE',  ( -64.52287095715006160, -23.47596703998600631, 11.44779298504228926 ) ) ;
#34706=DIRECTION ( 'NONE',  ( 1.000000000000000000, 3.773278334444166432E-23, 8.201307841325785021E-29 ) ) ;
#34707=CARTESIAN_POINT ( 'NONE',  ( -86.52287095715006160, -24.65952944569304606, 1.056160979905700570 ) ) ;
#34709=ORIENTED_EDGE ( 'NONE', *, *, #68908, .T. ) ;
#34710=CARTESIAN_POINT ( 'NONE',  ( -117.6228709571500559, -23.48783264082479505, -1.443836473390058384 ) ) ;
#34712=CARTESIAN_POINT ( 'NONE',  ( -51.52287095715006160, -23.94994826722565406, -0.6494450866342730277 ) ) ;
#34713=CARTESIAN_POINT ( 'NONE',  ( 20.52540449432101610, 0.9483640940595650104, -1.500000000000002220 ) ) ;
#34714=EDGE_LOOP ( 'NONE', ( #15643, #85638, #90523, #69100 ) ) ;
#34715=DIRECTION ( 'NONE',  ( -3.773278334453079618E-23, 0.9999999999976377785, 2.173523156925979975E-06 ) ) ;
#34717=CARTESIAN_POINT ( 'NONE',  ( -88.88918693012686845, -25.23397913219354649, 6.409327625488847602 ) ) ;
#34718=CARTESIAN_POINT ( 'NONE',  ( -2.938769918389303459, -22.12206158279486345, -1.500000000000002220 ) ) ;
#34720=PLANE ( 'NONE',  #40011 ) ;
#34721=EDGE_CURVE ( 'NONE', #40304, #4416, #92572, .T. ) ;
#34723=CARTESIAN_POINT ( 'NONE',  ( -42.62287095715002749, -24.50216790748098461, 0.6166512839513551558 ) ) ;
#34724=CARTESIAN_POINT ( 'NONE',  ( -119.6228709571500417, -24.65952944569304961, 1.056160979905704789 ) ) ;
#34725=B_SPLINE_CURVE_WITH_KNOTS ( 'NONE', 3,
 ( #92216, #92707, #67904, #6490, #90726, #15095 ),
 .UNSPECIFIED., .F., .F.,
 ( 4, 2, 4 ),
 ( 6.391158118952235087E-06, 0.001387004593080770967, 0.002767618028042589419 ),
 .UNSPECIFIED. ) ;
#34726=CARTESIAN_POINT ( 'NONE',  ( -20.82246440549779720, 1.468558417816581807, -1.500000000000002220 ) ) ;
#34727=ORIENTED_EDGE ( 'NONE', *, *, #98529, .F. ) ;
#34728=VECTOR ( 'NONE', #97923, 1000.000000000000227 ) ;
#34729=CARTESIAN_POINT ( 'NONE',  ( -40.25462936170517025, -25.11181042176191980, 2.840493060246056523 ) ) ;
#34730=ORIENTED_EDGE ( 'NONE', *, *, #65771, .F. ) ;
#34731=B_SPLINE_CURVE_WITH_KNOTS ( 'NONE', 3,
 ( #98840, #68899, #91728, #53691, #30332, #36450 ),
 .UNSPECIFIED., .F., .F.,
 ( 4, 2, 4 ),
 ( 1.570887131795413739E-05, 0.001396322306279765843, 0.002776935741241577573 ),
 .UNSPECIFIED. ) ;
#34733=EDGE_CURVE ( 'NONE', #75066, #92960, #32025, .T. ) ;
#34734=CARTESIAN_POINT ( 'NONE',  ( -33.62287095715005592, -23.47593901973091235, -1.443836447539013301 ) ) ;
#34735=CARTESIAN_POINT ( 'NONE',  ( -12.45680796028966597, 17.00782699154285638, -1.500000000000002220 ) ) ;
#34742=CARTESIAN_POINT ( 'NONE',  ( 10.00111611332133421, -19.26892646806700071, -1.500000000000002220 ) ) ;
#34743=CARTESIAN_POINT ( 'NONE',  ( -108.5228709571500616, -23.47596703998600631, 11.44779298504228038 ) ) ;
#34744=CARTESIAN_POINT ( 'NONE',  ( -17.00426676922356606, 14.40147940013276973, 11.49999999999999645 ) ) ;
#34745=ORIENTED_EDGE ( 'NONE', *, *, #75818, .T. ) ;
#34746=CARTESIAN_POINT ( 'NONE',  ( -51.39979512284951824, -25.31441837832753095, 5.729491880671105264 ) ) ;
#34748=CARTESIAN_POINT ( 'NONE',  ( -36.52287095715006870, -23.48786465467240347, 11.44779295918255180 ) ) ;
#34755=CARTESIAN_POINT ( 'NONE',  ( -121.5213660948649164, -23.73766607897670866, -1.055555164236450905 ) ) ;
#34757=CARTESIAN_POINT ( 'NONE',  ( -35.52287095715007581, -23.84047902841601640, -0.8780736468305702092 ) ) ;
#34758=CARTESIAN_POINT ( 'NONE',  ( -32.62287095715004881, -23.73907113216990439, -1.053371485793237250 ) ) ;
#34760=CARTESIAN_POINT ( 'NONE',  ( -42.62287095715006302, -24.51387760970723662, 9.387446482453421837 ) ) ;
#34761=CARTESIAN_POINT ( 'NONE',  ( -3.561414601982806349, 22.15502443119318343, -1.500000000000002220 ) ) ;
#34766=EDGE_CURVE ( 'NONE', #11431, #14117, #45455, .T. ) ;
#34767=EDGE_CURVE ( 'NONE', #36722, #66916, #756, .T. ) ;
#34768=CARTESIAN_POINT ( 'NONE',  ( -125.5228709571500900, -24.15431212366837244, -0.2830839119329186526 ) ) ;
#34769=EDGE_CURVE ( 'NONE', #2264, #81363, #6872, .T. ) ;
#34770=B_SPLINE_CURVE_WITH_KNOTS ( 'NONE', 3,
 ( #59386, #51777, #44661, #5591, #74599, #43172 ),
 .UNSPECIFIED., .F., .F.,
 ( 4, 2, 4 ),
 ( 0.000000000000000000, 0.001380901958385382473, 0.002761803916770764946 ),
 .UNSPECIFIED. ) ;
#34771=CARTESIAN_POINT ( 'NONE',  ( -97.25161593912366698, -24.37907397113049868, 9.703205396196697308 ) ) ;
#34772=CARTESIAN_POINT ( 'NONE',  ( 10.47639735327893362, 16.54961352017854637, -1.500000000000002220 ) ) ;
#34774=ORIENTED_EDGE ( 'NONE', *, *, #48148, .F. ) ;
#34775=EDGE_CURVE ( 'NONE', #55675, #17192, #12614, .T. ) ;
#34776=AXIS2_PLACEMENT_3D ( 'NONE', #35901, #88203, #89199 ) ;
#34777=CARTESIAN_POINT ( 'NONE',  ( 13.04721882220160012, 17.14300067834640373, 11.49999999999998934 ) ) ;
#34778=CARTESIAN_POINT ( 'NONE',  ( -128.5553793226067398, -24.65952944569305316, 1.056160979905708341 ) ) ;
#34779=CARTESIAN_POINT ( 'NONE',  ( -71.30457154551153565, -25.12218950775439197, 6.209207676158021272 ) ) ;
#34782=CARTESIAN_POINT ( 'NONE',  ( -22.77861398648627400, -3.026084143414268013, -1.500000000000002220 ) ) ;
#34785=CARTESIAN_POINT ( 'NONE',  ( -49.65271201290308767, -23.73766607897670156, -1.055555164236457344 ) ) ;
#34786=CARTESIAN_POINT ( 'NONE',  ( -0.3114230556345199963, -20.10660241673355486, 11.49999999999999645 ) ) ;
#34787=CARTESIAN_POINT ( 'NONE',  ( -68.62287095715005592, -23.47596703998600631, 11.44779298504227505 ) ) ;
#34788=CARTESIAN_POINT ( 'NONE',  ( -32.58669467011947773, -24.35071581493542681, 9.817618358456035921 ) ) ;
#34789=B_SPLINE_CURVE_WITH_KNOTS ( 'NONE', 3,
 ( #24225, #72420, #33843, #48079, #86127, #79005 ),
 .UNSPECIFIED., .F., .F.,
 ( 4, 2, 4 ),
 ( 0.000000000000000000, 0.001380901958385387894, 0.002761803916770775788 ),
 .UNSPECIFIED. ) ;
#34790=DIRECTION ( 'NONE',  ( -0.000000000000000000, 2.173523156925979552E-06, -0.9999999999976378895 ) ) ;
#34793=ADVANCED_FACE ( 'NONE', ( #68779 ), #25487, .T. ) ;
#34794=CARTESIAN_POINT ( 'NONE',  ( -19.08307359429613825, -5.530936995296134917, 11.49999999999998934 ) ) ;
#34795=ADVANCED_FACE ( 'NONE', ( #17481 ), #1271, .T. ) ;
#34797=CARTESIAN_POINT ( 'NONE',  ( -17.00503767097633556, -9.977476526402845991, -1.500000000000002220 ) ) ;
#34801=CARTESIAN_POINT ( 'NONE',  ( -115.6228709571500559, -24.82558206586148586, 1.605769216559630230 ) ) ;
#34802=CARTESIAN_POINT ( 'NONE',  ( -79.52287095715007581, -23.72773821059536914, 11.05748984161097503 ) ) ;
#34803=CARTESIAN_POINT ( 'NONE',  ( -19.87711886888390822, 5.503898473480427711, 11.49999999999999645 ) ) ;
#34804=EDGE_CURVE ( 'NONE', #2526, #29468, #25918, .T. ) ;
#34806=CARTESIAN_POINT ( 'NONE',  ( -4.753580043990282888, 22.13494492317406070, 11.49999999999999645 ) ) ;
#34807=ORIENTED_EDGE ( 'NONE', *, *, #8741, .T. ) ;
#34809=CARTESIAN_POINT ( 'NONE',  ( -51.29687923781919068, -25.27367468601215350, 3.993462154588707680 ) ) ;
#34810=CARTESIAN_POINT ( 'NONE',  ( -127.5228709571500616, -24.33927499327856125, 9.819080762295806508 ) ) ;
#34813=DIRECTION ( 'NONE',  ( 0.000000000000000000, -2.173523156925979552E-06, 0.9999999999976378895 ) ) ;
#34814=ORIENTED_EDGE ( 'NONE', *, *, #21239, .F. ) ;
#34818=CARTESIAN_POINT ( 'NONE',  ( 13.72848742581335912, -18.28091200367991576, -1.500000000000002220 ) ) ;
#34820=EDGE_CURVE ( 'NONE', #86130, #55078, #33205, .T. ) ;
#34822=CARTESIAN_POINT ( 'NONE',  ( -76.55620429048342146, -23.48786465467241058, 11.44779295918254469 ) ) ;
#34823=CARTESIAN_POINT ( 'NONE',  ( -18.84819291449097278, 12.34854029719970825, 11.49999999999999645 ) ) ;
#34824=ORIENTED_EDGE ( 'NONE', *, *, #15429, .T. ) ;
#34825=CARTESIAN_POINT ( 'NONE',  ( -43.58152581000473447, -24.51314013834316086, 0.6176544820404145097 ) ) ;
#34826=B_SPLINE_CURVE_WITH_KNOTS ( 'NONE', 3,
 ( #74942, #92174, #30782, #21652, #30273, #69346 ),
 .UNSPECIFIED., .F., .F.,
 ( 4, 2, 4 ),
 ( 0.000000000000000000, 0.001380764517853253371, 0.002761529035706506742 ),
 .UNSPECIFIED. ) ;
#34827=CARTESIAN_POINT ( 'NONE',  ( -8.471812324360341151, -20.26817064352238162, 11.49999999999998934 ) ) ;
#34828=CARTESIAN_POINT ( 'NONE',  ( -92.62287095715005592, -29.50250243563736774, 8.947779886222139822 ) ) ;
#34829=CARTESIAN_POINT ( 'NONE',  ( -29.21998272650427708, -25.21724568626827079, 5.646413213696420463 ) ) ;
#34830=ORIENTED_EDGE ( 'NONE', *, *, #65447, .T. ) ;
#34831=EDGE_CURVE ( 'NONE', #40253, #45491, #48946, .T. ) ;
#34832=CARTESIAN_POINT ( 'NONE',  ( -63.62287095715006302, -24.50321055353805377, 9.387540953477527594 ) ) ;
#34834=ORIENTED_EDGE ( 'NONE', *, *, #39150, .T. ) ;
#34835=CARTESIAN_POINT ( 'NONE',  ( -49.55620429048339304, -23.48786465467241058, 11.44779295918254647 ) ) ;
#34836=CARTESIAN_POINT ( 'NONE',  ( -11.60840874443078263, -16.91462557209307960, -1.500000000000002220 ) ) ;
#34837=ORIENTED_EDGE ( 'NONE', *, *, #81448, .F. ) ;
#34839=ORIENTED_EDGE ( 'NONE', *, *, #39671, .T. ) ;
#34841=CARTESIAN_POINT ( 'NONE',  ( 11.75533340255842596, 19.88161105567325038, 11.49999999999998934 ) ) ;
#34842=CARTESIAN_POINT ( 'NONE',  ( -41.52287095715008292, -24.51387760970724372, 9.387446482453407626 ) ) ;
#34843=CARTESIAN_POINT ( 'NONE',  ( 8.194921280291850962, -18.63391395107102610, -1.500000000000002220 ) ) ;
#34844=ORIENTED_EDGE ( 'NONE', *, *, #86852, .F. ) ;
#34846=CARTESIAN_POINT ( 'NONE',  ( -29.53070056818989286, -24.43102165026504835, 9.386484716961749797 ) ) ;
#34847=CARTESIAN_POINT ( 'NONE',  ( -105.6293832185014026, -24.40034930558991277, 0.3402023900116059041 ) ) ;
#34848=CARTESIAN_POINT ( 'NONE',  ( -71.18291627536595456, -25.03149790695943366, 7.291244984715597788 ) ) ;
#34849=ORIENTED_EDGE ( 'NONE', *, *, #1196, .F. ) ;
#34851=DIRECTION ( 'NONE',  ( -1.000000000000000000, -3.773278334444166432E-23, -8.201307841325785021E-29 ) ) ;
#34854=CARTESIAN_POINT ( 'NONE',  ( -9.565632364391108311, -18.43008791299702764, 11.49999999999998934 ) ) ;
#34855=VERTEX_POINT ( 'NONE', #16976 ) ;
#34856=CARTESIAN_POINT ( 'NONE',  ( -39.93825361760627857, -25.30561201263888194, 4.984140935953358387 ) ) ;
#34857=ORIENTED_EDGE ( 'NONE', *, *, #1144, .F. ) ;
#34859=CARTESIAN_POINT ( 'NONE',  ( -51.92991590564532345, -25.25550010977676507, 6.106957726396983865 ) ) ;
#34860=ORIENTED_EDGE ( 'NONE', *, *, #91804, .F. ) ;
#34862=CARTESIAN_POINT ( 'NONE',  ( -88.62287095715004170, -24.65952944569304606, 1.056160979905700570 ) ) ;
#34865=PLANE ( 'NONE',  #46961 ) ;
#34866=CARTESIAN_POINT ( 'NONE',  ( -43.53991149891938761, -24.35071581493542681, 9.817618358456032368 ) ) ;
#34867=CARTESIAN_POINT ( 'NONE',  ( 15.76968270297436625, 15.47746201419723100, 11.49999999999999645 ) ) ;
#34868=ORIENTED_EDGE ( 'NONE', *, *, #53572, .F. ) ;
#34869=CARTESIAN_POINT ( 'NONE',  ( -103.5550949855981031, -23.96119346886881019, -0.6495511937832079141 ) ) ;
#34870=CARTESIAN_POINT ( 'NONE',  ( 15.43685675143394498, -16.52047792065556564, -1.500000000000002220 ) ) ;
#34871=CARTESIAN_POINT ( 'NONE',  ( -115.5877643602478884, -24.83644354573579349, 8.397322867130093016 ) ) ;
#34873=ORIENTED_EDGE ( 'NONE', *, *, #88092, .T. ) ;
#34874=CARTESIAN_POINT ( 'NONE',  ( -75.62287095715005592, -25.00158670708909625, 2.256160236439166855 ) ) ;
#34875=AXIS2_PLACEMENT_3D ( 'NONE', #62243, #69848, #1342 ) ;
#34876=ADVANCED_FACE ( 'NONE', ( #10875 ), #78863, .F. ) ;
#34879=CARTESIAN_POINT ( 'NONE',  ( -21.01389645921736360, -2.595061309317715281, 11.49999999999998934 ) ) ;
#34882=LINE ( 'NONE', #88175, #21073 ) ;
#34883=CARTESIAN_POINT ( 'NONE',  ( -0.5504121640580519337, 22.28327991085032878, -1.500000000000002220 ) ) ;
#34885=CARTESIAN_POINT ( 'NONE',  ( -46.62287095715004881, -24.64898659630528499, 1.056161002820821038 ) ) ;
#34886=VECTOR ( 'NONE', #73430, 1000.000000000000114 ) ;
#34888=ORIENTED_EDGE ( 'NONE', *, *, #74682, .F. ) ;
#34889=CARTESIAN_POINT ( 'NONE',  ( -52.52287095715006870, -29.50247984919015209, -1.443849546365058689 ) ) ;
#34891=EDGE_CURVE ( 'NONE', #16731, #20987, #82873, .T. ) ;
#34892=AXIS2_PLACEMENT_3D ( 'NONE', #66800, #97721, #28212 ) ;
#34894=CARTESIAN_POINT ( 'NONE',  ( -71.58953762381672448, -23.48783264082478084, -1.443836473390067487 ) ) ;
#34896=CARTESIAN_POINT ( 'NONE',  ( -16.58133674543539371, -10.29093563426468450, -1.500000000000002220 ) ) ;
#34897=CARTESIAN_POINT ( 'NONE',  ( 14.45597713831175035, -15.85640774750547344, -1.500000000000002220 ) ) ;
#34898=CARTESIAN_POINT ( 'NONE',  ( -27.55569643375672584, -24.92774666922491278, 1.631373448212198429 ) ) ;
#34899=CARTESIAN_POINT ( 'NONE',  ( -51.57779606109421877, -24.65952944569304250, 1.056160979905695463 ) ) ;
#34901=CARTESIAN_POINT ( 'NONE',  ( 22.20583189720066741, -5.198064566299082756, -1.500000000000002220 ) ) ;
#34903=CARTESIAN_POINT ( 'NONE',  ( -102.5529430821646173, -24.15543982623908192, -0.2315651400026460249 ) ) ;
#34904=CARTESIAN_POINT ( 'NONE',  ( -128.5228709571501042, -23.72747288104470442, -1.053458166803224572 ) ) ;
#34905=CARTESIAN_POINT ( 'NONE',  ( 17.47191945374660094, 9.613082372698542599, 11.49999999999999645 ) ) ;
#34906=FACE_OUTER_BOUND ( 'NONE', #78903, .T. ) ;
#34907=CARTESIAN_POINT ( 'NONE',  ( -39.65634080071149015, -23.73791477778911485, 11.05961554403170943 ) ) ;
#34909=ORIENTED_EDGE ( 'NONE', *, *, #46246, .F. ) ;
#34911=EDGE_CURVE ( 'NONE', #94949, #26877, #63504, .T. ) ;
#34913=CARTESIAN_POINT ( 'NONE',  ( 14.13103794885040898, -16.47871000921984219, 11.49999999999998934 ) ) ;
#34914=CARTESIAN_POINT ( 'NONE',  ( -93.58953762381673869, -24.65952944569305316, 1.056160979905705011 ) ) ;
#34915=CARTESIAN_POINT ( 'NONE',  ( -18.05301863641116000, -7.546005365994440162, -1.500000000000002220 ) ) ;
#34917=EDGE_CURVE ( 'NONE', #14136, #58437, #6684, .T. ) ;
#34919=AXIS2_PLACEMENT_3D ( 'NONE', #17956, #35682, #48917 ) ;
#34921=CARTESIAN_POINT ( 'NONE',  ( -20.42006937447004233, 0.3101567295262241952, 11.49999999999999645 ) ) ;
#34923=CARTESIAN_POINT ( 'NONE',  ( -61.59189125704995860, -25.07259839747099051, 7.371166918563575976 ) ) ;
#34924=EDGE_LOOP ( 'NONE', ( #25119, #49102, #71784, #64224 ) ) ;
#34925=CARTESIAN_POINT ( 'NONE',  ( -127.5228709571500616, -29.50248528299804818, 1.056150453629047137 ) ) ;
#34926=CARTESIAN_POINT ( 'NONE',  ( -34.62287095715005592, -24.65952944569303895, 1.056160979905691688 ) ) ;
#34927=CARTESIAN_POINT ( 'NONE',  ( -116.5158230194428342, -24.66019654487199730, 8.947790411086115725 ) ) ;
#34928=CARTESIAN_POINT ( 'NONE',  ( -31.52166505407126706, -24.87479601683088148, 8.247789944647562876 ) ) ;
#34932=CARTESIAN_POINT ( 'NONE',  ( 3.792298468851710069, -22.70151372599487871, 11.49999999999999645 ) ) ;
#34933=CARTESIAN_POINT ( 'NONE',  ( -6.081610112697643622, 21.96313418072945822, 11.49999999999998934 ) ) ;
#34934=CARTESIAN_POINT ( 'NONE',  ( -110.6248242805079656, -24.83644354573579349, 8.397322867130096569 ) ) ;
#34937=CARTESIAN_POINT ( 'NONE',  ( -52.92287095715007439, -23.47593901973090169, -1.443836447538997980 ) ) ;
#34938=CARTESIAN_POINT ( 'NONE',  ( -110.6352815603598572, -23.48783264082476663, -1.443836473390091690 ) ) ;
#34940=CARTESIAN_POINT ( 'NONE',  ( -8.129759772327192380, 20.32010563749377141, 11.49999999999998934 ) ) ;
#34945=CARTESIAN_POINT ( 'NONE',  ( -96.52287095715010423, -23.95044443724993144, 10.65354141964648882 ) ) ;
#34946=ORIENTED_EDGE ( 'NONE', *, *, #2880, .T. ) ;
#34947=CARTESIAN_POINT ( 'NONE',  ( -19.05221060042639536, -7.346018566486852031, -1.500000000000002220 ) ) ;
#34950=ORIENTED_EDGE ( 'NONE', *, *, #92034, .T. ) ;
#34952=VERTEX_POINT ( 'NONE', #36703 ) ;
#34953=CARTESIAN_POINT ( 'NONE',  ( 20.85440106035463970, 9.703512019146668166, -1.500000000000002220 ) ) ;
#34955=CARTESIAN_POINT ( 'NONE',  ( 2.654622155064554789, -19.98241913370796041, -1.500000000000002220 ) ) ;
#34958=DIRECTION ( 'NONE',  ( 0.000000000000000000, -2.173523156925979552E-06, 0.9999999999976378895 ) ) ;
#34961=B_SPLINE_CURVE_WITH_KNOTS ( 'NONE', 3,
 ( #88582, #41405, #89077, #51020, #12440, #79957 ),
 .UNSPECIFIED., .F., .F.,
 ( 4, 2, 4 ),
 ( 0.000000000000000000, 0.001380901958385387894, 0.002761803916770775788 ),
 .UNSPECIFIED. ) ;
#34962=CARTESIAN_POINT ( 'NONE',  ( -95.63008670059350891, -24.52300882791530512, 0.6510814631126408125 ) ) ;
#34964=CARTESIAN_POINT ( 'NONE',  ( -14.55006661338671847, 15.66751491618662406, 11.49999999999999645 ) ) ;
#34965=ORIENTED_EDGE ( 'NONE', *, *, #5093, .T. ) ;
#34966=LINE ( 'NONE', #5010, #80848 ) ;
#34968=CARTESIAN_POINT ( 'NONE',  ( 21.95989154999629278, -3.605859658025859282, 11.49999999999998934 ) ) ;
#34969=CARTESIAN_POINT ( 'NONE',  ( 18.27903665858761073, 9.701928907310005457, -1.500000000000002220 ) ) ;
#34971=B_SPLINE_CURVE_WITH_KNOTS ( 'NONE', 3,
 ( #7081, #14182, #82705, #61385 ),
 .UNSPECIFIED., .F., .F.,
 ( 4, 4 ),
 ( 0.000000000000000000, 9.999999999998897304E-05 ),
 .UNSPECIFIED. ) ;
#34972=CARTESIAN_POINT ( 'NONE',  ( -71.72619204561506479, -25.20650855361216713, 6.812664954086296021 ) ) ;
#34975=ORIENTED_EDGE ( 'NONE', *, *, #56534, .F. ) ;
#34977=CARTESIAN_POINT ( 'NONE',  ( -20.86263692406621928, 1.606387762444034362, -1.500000000000002220 ) ) ;
#34978=CARTESIAN_POINT ( 'NONE',  ( 4.863445656156933694, -21.36585520573490626, 11.49999999999999645 ) ) ;
#34979=CARTESIAN_POINT ( 'NONE',  ( -26.50032570333037185, -24.89279848742383194, 6.891654722310369685 ) ) ;
#34980=CARTESIAN_POINT ( 'NONE',  ( -15.68175098440391402, -16.16561365185589594, 11.49999999999998934 ) ) ;
#34981=CARTESIAN_POINT ( 'NONE',  ( -2.368302597431856782, 20.80102113048726409, -1.500000000000002220 ) ) ;
#34982=DIRECTION ( 'NONE',  ( 1.000000000000000000, 3.773278334444166432E-23, 8.201307841325785021E-29 ) ) ;
#34984=CARTESIAN_POINT ( 'NONE',  ( -72.62287095715005592, -23.47593901973091235, -1.443836447539006196 ) ) ;
#34985=CARTESIAN_POINT ( 'NONE',  ( -126.5895376238167529, -24.66019654487199375, 8.947790411086124607 ) ) ;
#34986=ORIENTED_EDGE ( 'NONE', *, *, #47750, .F. ) ;
#34987=ORIENTED_EDGE ( 'NONE', *, *, #54019, .T. ) ;
#34988=VERTEX_POINT ( 'NONE', #28588 ) ;
#34989=CARTESIAN_POINT ( 'NONE',  ( -52.64484739509910582, -23.96119346886881019, -0.6495511937831939253 ) ) ;
#34990=ORIENTED_EDGE ( 'NONE', *, *, #79863, .T. ) ;
#34991=CARTESIAN_POINT ( 'NONE',  ( 19.99082695160776169, -7.785253749782737209, -1.500000000000002220 ) ) ;
#34994=VERTEX_POINT ( 'NONE', #12853 ) ;
#34995=CARTESIAN_POINT ( 'NONE',  ( 17.90021246794804810, -11.17811638239879279, 11.49999999999998934 ) ) ;
#34996=CARTESIAN_POINT ( 'NONE',  ( -69.86226356453386188, -25.11033435731149055, 2.832404375966413479 ) ) ;
#34997=EDGE_CURVE ( 'NONE', #79255, #937, #65847, .T. ) ;
#34998=CARTESIAN_POINT ( 'NONE',  ( -71.62287095715005592, -29.50250243563736774, 8.947779886222143375 ) ) ;
#34999=CARTESIAN_POINT ( 'NONE',  ( -121.5228709571500190, -24.66019654487199730, 8.947790411086119278 ) ) ;
#35000=CARTESIAN_POINT ( 'NONE',  ( -80.48373552459977986, -25.29534346072172823, 4.508937073655467032 ) ) ;
#35001=CARTESIAN_POINT ( 'NONE',  ( -129.5896970873678242, -24.35071581493544457, 9.817618358456021710 ) ) ;
#35002=CARTESIAN_POINT ( 'NONE',  ( 2.710298230372018669, -21.94706154713207980, -1.500000000000002220 ) ) ;
#35003=ORIENTED_EDGE ( 'NONE', *, *, #40279, .T. ) ;
#35004=CARTESIAN_POINT ( 'NONE',  ( -81.62948795153646131, -24.35071581493543391, 9.817618358456037697 ) ) ;
#35007=CARTESIAN_POINT ( 'NONE',  ( -41.71489324084514294, -25.27955919863082812, 4.846374523598886874 ) ) ;
#35010=FACE_OUTER_BOUND ( 'NONE', #18239, .T. ) ;
#35011=B_SPLINE_CURVE_WITH_KNOTS ( 'NONE', 3,
 ( #8879, #84571, #93683, #69356, #86576, #24665, #16054, #100272, #22658, #85572, #92183, #47026, #39404, #15559 ),
 .UNSPECIFIED., .F., .F.,
 ( 4, 2, 2, 2, 2, 2, 4 ),
 ( 0.000000000000000000, 0.0001867446169474697279, 0.0003734892338949394558, 0.0007469784677898988609, 0.001120467701684858212, 0.001307212318632341519, 0.001493956935579824827 ),
 .UNSPECIFIED. ) ;
#35012=EDGE_CURVE ( 'NONE', #80512, #62158, #43821, .T. ) ;
#35013=CARTESIAN_POINT ( 'NONE',  ( -47.58953762381672448, -24.64898659630367916, 1.056161002820380279 ) ) ;
#35014=CARTESIAN_POINT ( 'NONE',  ( -13.85510387911049079, -16.26762222697724880, -1.500000000000002220 ) ) ;
#35016=EDGE_CURVE ( 'NONE', #22424, #65090, #75500, .T. ) ;
#35017=B_SPLINE_CURVE_WITH_KNOTS ( 'NONE', 3,
 ( #1541, #18257, #87775, #95879 ),
 .UNSPECIFIED., .F., .F.,
 ( 4, 4 ),
 ( 0.000000000000000000, 9.999999999998206125E-05 ),
 .UNSPECIFIED. ) ;
#35018=FACE_OUTER_BOUND ( 'NONE', #2903, .T. ) ;
#35020=CARTESIAN_POINT ( 'NONE',  ( -64.56596816803553907, -23.48786465467241058, 11.44779295918254824 ) ) ;
#35021=CARTESIAN_POINT ( 'NONE',  ( -80.48900664166535535, -25.12298712672050982, 7.101635559041870494 ) ) ;
#35022=CARTESIAN_POINT ( 'NONE',  ( 15.50834587592193259, -16.38432980155966590, -1.500000000000002220 ) ) ;
#35027=LINE ( 'NONE', #18786, #38476 ) ;
#35028=CARTESIAN_POINT ( 'NONE',  ( -79.58202583663157270, -24.65952944569304606, 1.056160979905701902 ) ) ;
#35029=CARTESIAN_POINT ( 'NONE',  ( -18.83419513347712737, -5.836681878196540829, 11.49999999999999645 ) ) ;
#35031=AXIS2_PLACEMENT_3D ( 'NONE', #71723, #87944, #2218 ) ;
#35032=CARTESIAN_POINT ( 'NONE',  ( -67.62364343387676513, -24.65952944569304961, 1.056160979905700570 ) ) ;
#35036=CARTESIAN_POINT ( 'NONE',  ( -29.31644179857717347, -24.60094090469272743, 2.549175303124721292 ) ) ;
#35037=CARTESIAN_POINT ( 'NONE',  ( -101.0369185477202336, -25.12268536277769471, 6.965963272030491815 ) ) ;
#35038=CARTESIAN_POINT ( 'NONE',  ( -18.67883320684159543, -10.89015303950203517, 11.49999999999998934 ) ) ;
#35039=CARTESIAN_POINT ( 'NONE',  ( -126.6228709571499991, -24.33927499327855415, 9.819080762295802955 ) ) ;
#35041=CARTESIAN_POINT ( 'NONE',  ( -1.428710472040144452, 19.32843595812722626, -1.500000000000002220 ) ) ;
#35043=DIRECTION ( 'NONE',  ( -3.773278334453079618E-23, 0.9999999999976377785, 2.173523156925979975E-06 ) ) ;
#35044=CARTESIAN_POINT ( 'NONE',  ( 13.37688099249405127, 14.58279310912311111, -1.500000000000002220 ) ) ;
#35045=ORIENTED_EDGE ( 'NONE', *, *, #47496, .T. ) ;
#35046=CARTESIAN_POINT ( 'NONE',  ( -18.77428246231291808, -7.638711222589018135, 11.49999999999999645 ) ) ;
#35048=CARTESIAN_POINT ( 'NONE',  ( -41.62287095715006302, -29.50250786944525672, 11.44777988621624232 ) ) ;
#35050=CARTESIAN_POINT ( 'NONE',  ( -99.53087172303294494, -25.26929610620923228, 4.063316286417863132 ) ) ;
#35054=CARTESIAN_POINT ( 'NONE',  ( -71.62287095715002749, -24.33832256527048088, 0.1851278514138635367 ) ) ;
#35055=CARTESIAN_POINT ( 'NONE',  ( -4.446071851354966853, 19.53225066162704948, -1.500000000000002220 ) ) ;
#35056=B_SPLINE_CURVE_WITH_KNOTS ( 'NONE', 3,
 ( #86806, #24406, #9180, #94919, #71096, #78178 ),
 .UNSPECIFIED., .F., .F.,
 ( 4, 2, 4 ),
 ( 0.000000000000000000, 0.001380901958385397218, 0.002761803916770794436 ),
 .UNSPECIFIED. ) ;
#35057=CARTESIAN_POINT ( 'NONE',  ( -124.6228709571500559, -29.50250786944525672, 11.44777988621622811 ) ) ;
#35059=B_SPLINE_CURVE_WITH_KNOTS ( 'NONE', 3,
 ( #24825, #33441, #95843, #1509 ),
 .UNSPECIFIED., .F., .F.,
 ( 4, 4 ),
 ( 0.000000000000000000, 1.000000000000000000 ),
 .UNSPECIFIED. ) ;
#35060=CARTESIAN_POINT ( 'NONE',  ( -82.62287095715005592, -29.50247984919015209, -1.443849546365053582 ) ) ;
#35061=B_SPLINE_CURVE_WITH_KNOTS ( 'NONE', 3,
 ( #37922, #355, #54656, #68377, #22179, #99791 ),
 .UNSPECIFIED., .F., .F.,
 ( 4, 2, 4 ),
 ( 0.000000000000000000, 0.001380901958385381606, 0.002761803916770763211 ),
 .UNSPECIFIED. ) ;
#35062=CARTESIAN_POINT ( 'NONE',  ( -127.5228709571500616, -23.94994826722565406, -0.6494450866342692530 ) ) ;
#35063=CARTESIAN_POINT ( 'NONE',  ( -79.35172094158247091, -25.27805121895104534, 5.822999711083195251 ) ) ;
#35065=CARTESIAN_POINT ( 'NONE',  ( -73.50297087286094211, -24.34968618360933590, 0.1864209137778806424 ) ) ;
#35070=ORIENTED_EDGE ( 'NONE', *, *, #5842, .T. ) ;
#35071=CARTESIAN_POINT ( 'NONE',  ( 18.91379238805564356, 7.493326543281090935, 11.49999999999998934 ) ) ;
#35072=ORIENTED_EDGE ( 'NONE', *, *, #33540, .T. ) ;
#35073=CARTESIAN_POINT ( 'NONE',  ( -22.40196285382242536, -4.882868457752029379, 11.49999999999998934 ) ) ;
#35074=CARTESIAN_POINT ( 'NONE',  ( -32.50393181231471118, -23.96119346886880663, -0.6495511937831992544 ) ) ;
#35075=ORIENTED_EDGE ( 'NONE', *, *, #70413, .T. ) ;
#35076=CARTESIAN_POINT ( 'NONE',  ( -49.22373291780066751, -25.29465393801191553, 4.480743166237341590 ) ) ;
#35077=AXIS2_PLACEMENT_3D ( 'NONE', #38396, #47021, #77939 ) ;
#35078=CARTESIAN_POINT ( 'NONE',  ( -49.84148113843717454, -25.12215395822629560, 6.992078084850652964 ) ) ;
#35079=CARTESIAN_POINT ( 'NONE',  ( -87.62287095715004170, -24.64898659630528854, 1.056161002820827921 ) ) ;
#35080=CARTESIAN_POINT ( 'NONE',  ( 7.993063233546146229, -19.64520799392144568, 11.49999999999999645 ) ) ;
#35081=CARTESIAN_POINT ( 'NONE',  ( -18.13406196532287140, 12.77545654309102474, 11.49999999999998934 ) ) ;
#35083=CARTESIAN_POINT ( 'NONE',  ( 17.26003113218828489, 11.23261964116016642, 11.49999999999998934 ) ) ;
#35084=ADVANCED_FACE ( 'NONE', ( #28098 ), #96599, .T. ) ;
#35085=AXIS2_PLACEMENT_3D ( 'NONE', #39660, #94955, #23934 ) ;
#35086=ORIENTED_EDGE ( 'NONE', *, *, #95473, .F. ) ;
#35087=DIRECTION ( 'NONE',  ( -3.773278334453079618E-23, 0.9999999999976377785, 2.173523156925979975E-06 ) ) ;
#35088=ORIENTED_EDGE ( 'NONE', *, *, #42263, .F. ) ;
#35089=CARTESIAN_POINT ( 'NONE',  ( -36.92287095715006018, -23.47596703998600276, 11.44779298504227683 ) ) ;
#35091=VERTEX_POINT ( 'NONE', #98083 ) ;
#35096=CARTESIAN_POINT ( 'NONE',  ( -77.52287095715009002, -24.35013146730204170, 9.818937971375095941 ) ) ;
#35097=CARTESIAN_POINT ( 'NONE',  ( -71.55620429048337883, -24.64965694238574301, 8.947790433994201820 ) ) ;
#35099=CARTESIAN_POINT ( 'NONE',  ( 18.78520451414993531, -8.817701518030307994, -1.500000000000002220 ) ) ;
#35100=B_SPLINE_CURVE_WITH_KNOTS ( 'NONE', 3,
 ( #26896, #16025, #99749, #37879, #15526, #30252 ),
 .UNSPECIFIED., .F., .F.,
 ( 4, 2, 4 ),
 ( 0.000000000000000000, 0.0002698174196818396231, 0.0005396348393636792463 ),
 .UNSPECIFIED. ) ;
#35101=CARTESIAN_POINT ( 'NONE',  ( 19.96715809174937561, -8.635335823514383335, 11.49999999999999645 ) ) ;
#35102=ORIENTED_EDGE ( 'NONE', *, *, #84031, .T. ) ;
#35104=CARTESIAN_POINT ( 'NONE',  ( -115.5917283184090394, -24.15503026093916716, -0.2815557561904330486 ) ) ;
#35105=CARTESIAN_POINT ( 'NONE',  ( -22.05133119090760019, 4.102169094691678453, -1.500000000000002220 ) ) ;
#35107=LINE ( 'NONE', #68052, #1148 ) ;
#35108=CARTESIAN_POINT ( 'NONE',  ( -65.66192201872799217, -23.48783264082477018, -1.443836473390096353 ) ) ;
#35109=VERTEX_POINT ( 'NONE', #51936 ) ;
#35112=ORIENTED_EDGE ( 'NONE', *, *, #43922, .T. ) ;
#35115=ORIENTED_EDGE ( 'NONE', *, *, #18638, .F. ) ;
#35116=CARTESIAN_POINT ( 'NONE',  ( 17.78463046036513617, -11.72987588014745342, -1.500000000000002220 ) ) ;
#35118=CARTESIAN_POINT ( 'NONE',  ( -89.81226385320383088, -25.23397913219354649, 6.409327625488847602 ) ) ;
#35119=CARTESIAN_POINT ( 'NONE',  ( -11.22809577558575000, 18.72649003030000259, 11.49999999999998934 ) ) ;
#35120=CARTESIAN_POINT ( 'NONE',  ( -38.52287095715009002, -23.72773821059535848, 11.05748984161097326 ) ) ;
#35121=CARTESIAN_POINT ( 'NONE',  ( 19.67839991682829748, -11.23141783594569354, 11.49999999999998934 ) ) ;
#35123=CARTESIAN_POINT ( 'NONE',  ( -99.52287095715006160, -29.50250786944525672, 11.44777988621623166 ) ) ;
#35124=CARTESIAN_POINT ( 'NONE',  ( 19.95399986947220583, -8.914707708046476498, -1.500000000000002220 ) ) ;
#35126=ORIENTED_EDGE ( 'NONE', *, *, #31078, .T. ) ;
#35128=CARTESIAN_POINT ( 'NONE',  ( -73.62287095715005592, -24.64898659630367916, 1.056161002820824368 ) ) ;
#35129=EDGE_CURVE ( 'NONE', #30069, #95739, #73006, .T. ) ;
#35131=ORIENTED_EDGE ( 'NONE', *, *, #57250, .T. ) ;
#35132=CARTESIAN_POINT ( 'NONE',  ( -30.60851184801261837, -24.48743478789338468, 9.418369803765530790 ) ) ;
#35134=ADVANCED_FACE ( 'NONE', ( #53934 ), #92970, .T. ) ;
#35136=VECTOR ( 'NONE', #23884, 1000.000000000000114 ) ;
#35137=CARTESIAN_POINT ( 'NONE',  ( -120.6228709571500417, -23.47596703998600631, 11.44779298504227683 ) ) ;
#35138=CARTESIAN_POINT ( 'NONE',  ( -20.90244970016518877, -3.954922567530639199, 11.49999999999998934 ) ) ;
#35139=CARTESIAN_POINT ( 'NONE',  ( -30.49308942697465952, -23.47593901973084485, -1.443836476861628970 ) ) ;
#35140=EDGE_CURVE ( 'NONE', #63070, #50327, #37949, .T. ) ;
#35141=CARTESIAN_POINT ( 'NONE',  ( -27.08002768120591242, -24.75186003446978944, 2.428019306975902847 ) ) ;
#35142=CARTESIAN_POINT ( 'NONE',  ( -114.5228709571500616, -24.65952944569305316, 1.056160979905704123 ) ) ;
#35143=CARTESIAN_POINT ( 'NONE',  ( -84.62287095715005592, -24.66019654487199730, 8.947790411086128159 ) ) ;
#35144=CARTESIAN_POINT ( 'NONE',  ( -44.62287095715007013, -23.95044443724992078, 10.65354141964649237 ) ) ;
#35146=CARTESIAN_POINT ( 'NONE',  ( 3.994393897313025743, -19.14333888664780048, 11.49999999999999645 ) ) ;
#35150=ORIENTED_EDGE ( 'NONE', *, *, #51980, .T. ) ;
#35151=DIRECTION ( 'NONE',  ( -3.773278334453079618E-23, 0.9999999999976377785, 2.173523156925979975E-06 ) ) ;
#35152=CARTESIAN_POINT ( 'NONE',  ( -100.9051445215427947, -25.04466488984843764, 7.507873723526761189 ) ) ;
#35153=VECTOR ( 'NONE', #34540, 1000.000000000000114 ) ;
#35154=CARTESIAN_POINT ( 'NONE',  ( -51.58953762381672448, -23.48783264082478084, -1.443836473390070596 ) ) ;
#35155=CARTESIAN_POINT ( 'NONE',  ( -80.51244414166535535, -25.24813991317089545, 7.563173748558941867 ) ) ;
#35156=CARTESIAN_POINT ( 'NONE',  ( 0.7877182283408599162, 19.66719298131377514, -1.500000000000002220 ) ) ;
#35157=VERTEX_POINT ( 'NONE', #22451 ) ;
#35158=DIRECTION ( 'NONE',  ( -1.000000000000000000, -3.773278334444166432E-23, -8.201307841325785021E-29 ) ) ;
#35159=CARTESIAN_POINT ( 'NONE',  ( -118.5228709571501184, -23.48783264082477373, -1.443836473390083475 ) ) ;
#35160=VECTOR ( 'NONE', #33311, 1000.000000000000114 ) ;
#35162=B_SPLINE_CURVE_WITH_KNOTS ( 'NONE', 3,
 ( #82450, #75330, #91556, #14428 ),
 .UNSPECIFIED., .F., .F.,
 ( 4, 4 ),
 ( 0.000000000000000000, 9.999999999996123101E-05 ),
 .UNSPECIFIED. ) ;
#35165=DIRECTION ( 'NONE',  ( -3.773278334444167608E-23, 1.000000000000000000, 0.000000000000000000 ) ) ;
#35166=CARTESIAN_POINT ( 'NONE',  ( -69.62287095715005592, -23.94994826722515313, -0.6494450866351728635 ) ) ;
#35167=CARTESIAN_POINT ( 'NONE',  ( -118.5546855235172785, -24.15543982623907482, -0.2315651400026558782 ) ) ;
#35168=CARTESIAN_POINT ( 'NONE',  ( -80.90938632151146237, -25.31249729222309597, 5.276660411446114196 ) ) ;
#35172=DIRECTION ( 'NONE',  ( -3.773278334453079618E-23, 0.9999999999976377785, 2.173523156925979975E-06 ) ) ;
#35173=CARTESIAN_POINT ( 'NONE',  ( 18.80405327530603543, -6.659971710459020144, -1.500000000000002220 ) ) ;
#35174=CARTESIAN_POINT ( 'NONE',  ( -0.08148069157530678230, -21.99516841672774348, 10.01542119451336887 ) ) ;
#35175=CARTESIAN_POINT ( 'NONE',  ( 0.1862606309321278575, -19.90735222434816976, -1.500000000000002220 ) ) ;
#35176=ORIENTED_EDGE ( 'NONE', *, *, #92591, .T. ) ;
#35178=EDGE_CURVE ( 'NONE', #55445, #84745, #97264, .T. ) ;
#35181=CARTESIAN_POINT ( 'NONE',  ( -26.36173610263349687, -24.88504641058569433, 6.596543391192986938 ) ) ;
#35183=EDGE_CURVE ( 'NONE', #39855, #28152, #30077, .T. ) ;
#35184=CARTESIAN_POINT ( 'NONE',  ( -62.55620429048343567, -23.47596703998600276, 11.44779298504227505 ) ) ;
#35185=ORIENTED_EDGE ( 'NONE', *, *, #72263, .F. ) ;
#35187=LINE ( 'NONE', #66159, #22516 ) ;
#35189=B_SPLINE_CURVE_WITH_KNOTS ( 'NONE', 3,
 ( #17590, #55672, #33306, #64294, #24195, #32313, #867, #55171 ),
 .UNSPECIFIED., .F., .F.,
 ( 4, 2, 2, 4 ),
 ( -0.001240355328176873757, -0.0002398155169399556787, 0.0007607242942969623997, 0.002761803916770794003 ),
 .UNSPECIFIED. ) ;
#35190=CARTESIAN_POINT ( 'NONE',  ( 13.55758662847591900, -15.04642845256218031, -1.500000000000002220 ) ) ;
#35191=CARTESIAN_POINT ( 'NONE',  ( -68.97719918508434489, -25.28711388198359700, 5.838800831980617723 ) ) ;
#35193=AXIS2_PLACEMENT_3D ( 'NONE', #48351, #95011, #16378 ) ;
#35196=CARTESIAN_POINT ( 'NONE',  ( -80.43221577628075636, -25.31553502933635968, 4.967019755914117596 ) ) ;
#35198=CARTESIAN_POINT ( 'NONE',  ( -19.91332876899582160, 2.521106391696132931, -1.500000000000002220 ) ) ;
#35199=CARTESIAN_POINT ( 'NONE',  ( -1.027814097295878693, -20.98676634966329146, 11.49999999999999645 ) ) ;
#35200=VECTOR ( 'NONE', #63743, 1000.000000000000114 ) ;
#35202=CARTESIAN_POINT ( 'NONE',  ( -70.63224074161550448, -24.63419186844611275, 9.035850630976918652 ) ) ;
#35203=CARTESIAN_POINT ( 'NONE',  ( 5.627179592841175193, 21.36305014179116668, -1.500000000000002220 ) ) ;
#35205=CARTESIAN_POINT ( 'NONE',  ( -39.51244657141699435, -25.31589210260499101, 4.531907284092489441 ) ) ;
#35207=FACE_OUTER_BOUND ( 'NONE', #347, .T. ) ;
#35209=PLANE ( 'NONE',  #38128 ) ;
#35210=CARTESIAN_POINT ( 'NONE',  ( -31.61026445906011517, -23.73766607897669800, -1.055555164236445131 ) ) ;
#35211=ORIENTED_EDGE ( 'NONE', *, *, #56792, .F. ) ;
#35212=VERTEX_POINT ( 'NONE', #61552 ) ;
#35214=CARTESIAN_POINT ( 'NONE',  ( -125.5228709571500616, -23.47596703998600631, 11.44779298504227683 ) ) ;
#35215=CARTESIAN_POINT ( 'NONE',  ( -61.92287095715004597, -23.47593901973090169, -1.443836447538997758 ) ) ;
#35216=CARTESIAN_POINT ( 'NONE',  ( 20.45670835789597319, 2.398913822417158226, -1.500000000000002220 ) ) ;
#35217=CARTESIAN_POINT ( 'NONE',  ( 18.51311748589099082, 11.02308708543723270, 11.49999999999999645 ) ) ;
#35218=ORIENTED_EDGE ( 'NONE', *, *, #39225, .F. ) ;
#35223=CARTESIAN_POINT ( 'NONE',  ( -10.28394192611005842, 19.82837715243953625, -1.500000000000002220 ) ) ;
#35227=ORIENTED_EDGE ( 'NONE', *, *, #34378, .F. ) ;
#35230=CARTESIAN_POINT ( 'NONE',  ( 18.76864855846692492, -9.085702381504452418, 11.49999999999998934 ) ) ;
#35231=VERTEX_POINT ( 'NONE', #91475 ) ;
#35233=VERTEX_POINT ( 'NONE', #6742 ) ;
#35234=AXIS2_PLACEMENT_3D ( 'NONE', #27841, #72530, #56816 ) ;
#35235=ORIENTED_EDGE ( 'NONE', *, *, #22607, .F. ) ;
#35236=CARTESIAN_POINT ( 'NONE',  ( -100.5472794312289295, -24.73531770709095312, 8.716586749053508498 ) ) ;
#35237=CARTESIAN_POINT ( 'NONE',  ( 15.50021099394596646, 14.30638080151107694, -1.500000000000002220 ) ) ;
#35239=CARTESIAN_POINT ( 'NONE',  ( -28.52287095715005805, -24.48836230353387222, 1.056161703005638719 ) ) ;
#35240=CARTESIAN_POINT ( 'NONE',  ( -49.20721729649422826, -25.30221391860467151, 5.306624793317872957 ) ) ;
#35241=CARTESIAN_POINT ( 'NONE',  ( -120.5936535130245773, -23.48786465467241769, 11.44779295918253936 ) ) ;
#35243=CARTESIAN_POINT ( 'NONE',  ( -64.62287095715005592, -23.48786465467241413, 11.44779295918254824 ) ) ;
#35245=CARTESIAN_POINT ( 'NONE',  ( -21.36891742734480104, 3.643610035731704055, -1.500000000000002220 ) ) ;
#35246=CARTESIAN_POINT ( 'NONE',  ( -63.52287095715006160, -23.48786465467241058, 11.44779295918254824 ) ) ;
#35248=CARTESIAN_POINT ( 'NONE',  ( -16.22183044023116238, -15.26045173261249310, 11.49999999999999645 ) ) ;
#35249=ORIENTED_EDGE ( 'NONE', *, *, #36328, .T. ) ;
#35250=B_SPLINE_CURVE_WITH_KNOTS ( 'NONE', 3,
 ( #43507, #35883, #59227, #51616, #9292, #24016 ),
 .UNSPECIFIED., .F., .F.,
 ( 4, 2, 4 ),
 ( 1.570755371633718645E-05, 0.001396183895866086452, 0.002776660238015836012 ),
 .UNSPECIFIED. ) ;
#35251=CARTESIAN_POINT ( 'NONE',  ( -76.92287095715008149, -23.47593901973090524, -1.443836447538997980 ) ) ;
#35254=ORIENTED_EDGE ( 'NONE', *, *, #15557, .T. ) ;
#35255=B_SPLINE_CURVE_WITH_KNOTS ( 'NONE', 3,
 ( #75347, #82470, #98186, #81485 ),
 .UNSPECIFIED., .F., .F.,
 ( 4, 4 ),
 ( 0.1188422306059488676, 0.1198429776467144353 ),
 .UNSPECIFIED. ) ;
#35256=B_SPLINE_CURVE_WITH_KNOTS ( 'NONE', 3,
 ( #48340, #10269, #94999, #72181 ),
 .UNSPECIFIED., .F., .F.,
 ( 4, 4 ),
 ( 0.5909219629093517279, 0.5999283941814672616 ),
 .UNSPECIFIED. ) ;
#35258=ORIENTED_EDGE ( 'NONE', *, *, #47320, .F. ) ;
#35259=VERTEX_POINT ( 'NONE', #99573 ) ;
#35260=EDGE_CURVE ( 'NONE', #52403, #50453, #13672, .T. ) ;
#35261=CARTESIAN_POINT ( 'NONE',  ( -103.6228709571500417, -23.47596703998600631, 11.44779298504227860 ) ) ;
#35263=EDGE_CURVE ( 'NONE', #40347, #47659, #26985, .T. ) ;
#35264=CARTESIAN_POINT ( 'NONE',  ( -63.55620429048339304, -24.65952944569304606, 1.056160979905694131 ) ) ;
#35265=CARTESIAN_POINT ( 'NONE',  ( -87.52287095715006160, -23.95044443724992789, 10.65354141964649415 ) ) ;
#35267=ORIENTED_EDGE ( 'NONE', *, *, #39985, .F. ) ;
#35268=CARTESIAN_POINT ( 'NONE',  ( -9.899997732206244905, -16.63842163800745766, 11.49999999999999645 ) ) ;
#35270=CARTESIAN_POINT ( 'NONE',  ( -16.84940295534276800, 14.81145437567392698, -1.500000000000002220 ) ) ;
#35272=ORIENTED_EDGE ( 'NONE', *, *, #37206, .T. ) ;
#35276=PLANE ( 'NONE',  #44992 ) ;
#35277=CARTESIAN_POINT ( 'NONE',  ( -130.5728709571500588, -24.57143472585066846, 0.8294870405985542705 ) ) ;
#35278=CARTESIAN_POINT ( 'NONE',  ( -12.94911239430987315, -14.73082512860577609, -1.500000000000002220 ) ) ;
#35279=B_SPLINE_SURFACE_WITH_KNOTS ( 'NONE', 3, 3, ( 
 ( #77037, #7538, #38492, #69442 ),
 ( #31375, #1941, #9538, #32885 ),
 ( #85157, #62853, #16643, #48115 ),
 ( #79043, #46614, #55734, #93771 ),
 ( #71956, #77536, #63857, #2437 ),
 ( #24261, #61842, #23753, #23249 ),
 ( #54231, #94771, #78029, #55236 ) ),
 .UNSPECIFIED., .F., .F., .F.,
 ( 4, 3, 4 ),
 ( 4, 4 ),
 ( 0.3495694201709305671, 0.5199404137006313764, 0.6903114072303322413 ),
 ( 0.6891232925396537645, 0.7171688452333530028 ),
 .UNSPECIFIED. ) ;
#35280=CARTESIAN_POINT ( 'NONE',  ( -49.51094237493734340, -25.27738574500889257, 4.037618946434144540 ) ) ;
#35281=ORIENTED_EDGE ( 'NONE', *, *, #21227, .F. ) ;
#35282=CARTESIAN_POINT ( 'NONE',  ( -17.63906703526961550, 12.34593017946836291, -1.500000000000002220 ) ) ;
#35285=CARTESIAN_POINT ( 'NONE',  ( -71.01839045479064794, -25.25639544905377321, 6.841306829129303324 ) ) ;
#35286=CARTESIAN_POINT ( 'NONE',  ( -100.5228709571500900, -23.48783264082477018, -1.443836473390086583 ) ) ;
#35287=CARTESIAN_POINT ( 'NONE',  ( -128.6228709571500417, -29.50248528299804818, 1.056150453629047137 ) ) ;
#35288=CARTESIAN_POINT ( 'NONE',  ( -10.52143791818333085, 20.43947972196396989, -1.500000000000002220 ) ) ;
#35291=CARTESIAN_POINT ( 'NONE',  ( -49.49485161334624195, -24.34968618360933590, 0.1864209137778799485 ) ) ;
#35292=CARTESIAN_POINT ( 'NONE',  ( 17.00595499256408871, 10.69956108467327205, 11.49999999999999645 ) ) ;
#35294=CARTESIAN_POINT ( 'NONE',  ( -32.53787845003378720, -24.35071581493542681, 9.817618358456035921 ) ) ;
#35296=B_SPLINE_CURVE_WITH_KNOTS ( 'NONE', 3,
 ( #33675, #63641, #9323, #96073, #26055, #95072 ),
 .UNSPECIFIED., .F., .F.,
 ( 4, 2, 4 ),
 ( 0.000000000000000000, 0.001380901958385387894, 0.002761803916770775788 ),
 .UNSPECIFIED. ) ;
#35297=FACE_OUTER_BOUND ( 'NONE', #2606, .T. ) ;
#35299=DIRECTION ( 'NONE',  ( 3.773278334444166432E-23, -1.000000000000000000, 0.000000000000000000 ) ) ;
#35300=CARTESIAN_POINT ( 'NONE',  ( -13.97081141688431138, 14.13901428111770819, -1.500000000000002220 ) ) ;
#35301=B_SPLINE_CURVE_WITH_KNOTS ( 'NONE', 3,
 ( #74960, #59766, #27802, #66883, #44532, #75456 ),
 .UNSPECIFIED., .F., .F.,
 ( 4, 2, 4 ),
 ( 6.391158118955276782E-06, 0.001387004593080777256, 0.002767618028042598960 ),
 .UNSPECIFIED. ) ;
#35302=CARTESIAN_POINT ( 'NONE',  ( -113.5871619926412990, -24.65952944569305316, 1.056160979905705011 ) ) ;
#35303=CARTESIAN_POINT ( 'NONE',  ( -2.117704968268854682, 19.61795684621070990, -1.500000000000002220 ) ) ;
#35304=AXIS2_PLACEMENT_3D ( 'NONE', #58371, #10185, #4075 ) ;
#35306=CARTESIAN_POINT ( 'NONE',  ( -72.92287095715006728, -23.47596703998600631, 11.44779298504227860 ) ) ;
#35308=CARTESIAN_POINT ( 'NONE',  ( -18.80638259998596951, 8.471300643254643603, 11.49999999999999645 ) ) ;
#35310=DIRECTION ( 'NONE',  ( 0.000000000000000000, -2.173523156925980399E-06, 0.9999999999976378895 ) ) ;
#35311=CARTESIAN_POINT ( 'NONE',  ( 20.48348528492645571, -9.684159049092739835, 11.49999999999999645 ) ) ;
#35316=VECTOR ( 'NONE', #65992, 1000.000000000000114 ) ;
#35317=CARTESIAN_POINT ( 'NONE',  ( -27.12300167417273045, -24.61460094789499564, 8.164242432340882871 ) ) ;
#35318=CARTESIAN_POINT ( 'NONE',  ( -36.55620429048339304, -23.48783264082477373, -1.443836473390072372 ) ) ;
#35321=DIRECTION ( 'NONE',  ( -3.773278334453079030E-23, 0.9999999999976377785, 2.173523156925979128E-06 ) ) ;
#35322=CARTESIAN_POINT ( 'NONE',  ( -14.01358469492184966, -18.07645309290061064, 11.49999999999998934 ) ) ;
#35324=CARTESIAN_POINT ( 'NONE',  ( 19.31049906410359895, -9.575588319827552652, -1.500000000000002220 ) ) ;
#35327=CARTESIAN_POINT ( 'NONE',  ( -12.86601690267178100, 18.50254183665605012, 11.49999999999999645 ) ) ;
#35329=CARTESIAN_POINT ( 'NONE',  ( -29.23535468533444259, -25.19827913475990400, 4.357126516840850172 ) ) ;
#35330=CARTESIAN_POINT ( 'NONE',  ( 20.22059317821533853, 8.664326447042464352, -1.500000000000002220 ) ) ;
#35331=EDGE_CURVE ( 'NONE', #59549, #27337, #74246, .T. ) ;
#35333=CARTESIAN_POINT ( 'NONE',  ( -69.97769073112337423, -25.04188339297948218, 7.520920306927235011 ) ) ;
#35334=ORIENTED_EDGE ( 'NONE', *, *, #99, .F. ) ;
#35335=DIRECTION ( 'NONE',  ( -3.773278334453079618E-23, 0.9999999999976377785, 2.173523156925979975E-06 ) ) ;
#35336=DIRECTION ( 'NONE',  ( -3.773278334444166432E-23, 1.000000000000000000, 0.000000000000000000 ) ) ;
#35337=EDGE_LOOP ( 'NONE', ( #18793, #4801, #69004, #12630 ) ) ;
#35338=CARTESIAN_POINT ( 'NONE',  ( -84.62287095715004170, -24.33832256526968862, 0.1851278514119911178 ) ) ;
#35340=ORIENTED_EDGE ( 'NONE', *, *, #5717, .F. ) ;
#35341=ORIENTED_EDGE ( 'NONE', *, *, #67768, .T. ) ;
#35342=ORIENTED_EDGE ( 'NONE', *, *, #12424, .T. ) ;
#35343=LINE ( 'NONE', #20597, #12878 ) ;
#35345=LINE ( 'NONE', #50074, #6601 ) ;
#35346=CARTESIAN_POINT ( 'NONE',  ( -20.42006937447004233, 0.3101567295262241952, -1.500000000000002220 ) ) ;
#35348=CARTESIAN_POINT ( 'NONE',  ( -71.57279388816485266, -25.17182522529348532, 6.802880960782522912 ) ) ;
#35349=EDGE_CURVE ( 'NONE', #38339, #20357, #2156, .T. ) ;
#35350=CARTESIAN_POINT ( 'NONE',  ( -29.57432519004955296, -24.58082521808944421, 8.947790440257527678 ) ) ;
#35351=EDGE_CURVE ( 'NONE', #96258, #70136, #44069, .T. ) ;
#35352=B_SPLINE_CURVE_WITH_KNOTS ( 'NONE', 3,
 ( #72209, #87418, #95534, #40252 ),
 .UNSPECIFIED., .F., .F.,
 ( 4, 4 ),
 ( 0.000000000000000000, 9.999999999997510880E-05 ),
 .UNSPECIFIED. ) ;
#35353=CARTESIAN_POINT ( 'NONE',  ( -97.52287095715004739, -24.50216790748205398, 0.6166512839542558355 ) ) ;
#35354=CARTESIAN_POINT ( 'NONE',  ( -70.87191485471986141, -25.03149828777604213, 7.466452049494895604 ) ) ;
#35356=CARTESIAN_POINT ( 'NONE',  ( -28.29914910988898669, -25.21531691454156032, 2.427550070888207401 ) ) ;
#35357=FACE_OUTER_BOUND ( 'NONE', #61549, .T. ) ;
#35358=ADVANCED_FACE ( 'NONE', ( #93976 ), #63562, .T. ) ;
#35359=ORIENTED_EDGE ( 'NONE', *, *, #58676, .T. ) ;
#35360=CARTESIAN_POINT ( 'NONE',  ( -19.11632921840048738, -8.121837694355717119, 11.49999999999998934 ) ) ;
#35362=DIRECTION ( 'NONE',  ( 0.000000000000000000, -0.9999999999976377785, -2.173523156925979975E-06 ) ) ;
#35363=EDGE_LOOP ( 'NONE', ( #12015, #81554, #29362, #65313 ) ) ;
#35364=B_SPLINE_SURFACE_WITH_KNOTS ( 'NONE', 3, 3, ( 
 ( #16584, #64301, #39438, #54671 ),
 ( #17598, #47561, #25202, #78482 ),
 ( #55679, #31828, #85602, #93211 ),
 ( #63803, #17094, #25705, #2384 ),
 ( #8981, #33314, #48056, #95224 ),
 ( #56684, #78985, #86107, #87616 ),
 ( #71395, #16090, #77974, #18099 ) ),
 .UNSPECIFIED., .F., .F., .F.,
 ( 4, 3, 4 ),
 ( 4, 4 ),
 ( 0.7945040050992243641, 0.8970133687736507877, 0.9995227324480771003 ),
 ( 0.9597378799379333580, 0.9611936831856934260 ),
 .UNSPECIFIED. ) ;
#35365=PLANE ( 'NONE',  #24394 ) ;
#35366=CARTESIAN_POINT ( 'NONE',  ( -97.52287095715003318, -24.66019654487200441, 8.947790411086119278 ) ) ;
#35367=ORIENTED_EDGE ( 'NONE', *, *, #12539, .F. ) ;
#35368=EDGE_LOOP ( 'NONE', ( #48717, #11205, #36960, #94993 ) ) ;
#35369=CARTESIAN_POINT ( 'NONE',  ( -114.6228709571500701, -23.48783264082478794, -1.443836473390060382 ) ) ;
#35371=CARTESIAN_POINT ( 'NONE',  ( -86.52287095715009002, -23.72747288104470087, -1.053458166803225682 ) ) ;
#35372=CARTESIAN_POINT ( 'NONE',  ( -70.74035176281489612, -25.31201604152037987, 5.376055887764303876 ) ) ;
#35373=EDGE_CURVE ( 'NONE', #35718, #50270, #18536, .T. ) ;
#35374=CARTESIAN_POINT ( 'NONE',  ( -21.55788180805707555, 4.768121097544787190, 11.49999999999999645 ) ) ;
#35375=VERTEX_POINT ( 'NONE', #94482 ) ;
#35376=FACE_OUTER_BOUND ( 'NONE', #59287, .T. ) ;
#35377=CARTESIAN_POINT ( 'NONE',  ( 20.74359285767136640, 8.971229656761206428, 11.49999999999998934 ) ) ;
#35378=AXIS2_PLACEMENT_3D ( 'NONE', #47388, #45397, #55006 ) ;
#35379=CARTESIAN_POINT ( 'NONE',  ( -115.5161475269273836, -24.52399227489127043, 9.353111116836528183 ) ) ;
#35380=VERTEX_POINT ( 'NONE', #24966 ) ;
#35383=ADVANCED_FACE ( 'NONE', ( #55940 ), #72163, .T. ) ;
#35386=CARTESIAN_POINT ( 'NONE',  ( -57.60487676331112539, -23.73791477778911840, 11.05961554403170588 ) ) ;
#35388=CARTESIAN_POINT ( 'NONE',  ( -15.68702345270385834, -14.21367052863537417, -1.500000000000002220 ) ) ;
#35391=CARTESIAN_POINT ( 'NONE',  ( -41.68883930382232705, -25.30531595339526163, 4.893887653588548048 ) ) ;
#35392=CARTESIAN_POINT ( 'NONE',  ( -19.83904684311861644, 10.14288308415042827, -1.500000000000002220 ) ) ;
#35393=B_SPLINE_CURVE_WITH_KNOTS ( 'NONE', 3,
 ( #60410, #4113, #43179, #35563 ),
 .UNSPECIFIED., .F., .F.,
 ( 4, 4 ),
 ( 0.000000000000000000, 0.0001000000000000167422 ),
 .UNSPECIFIED. ) ;
#35395=ADVANCED_FACE ( 'NONE', ( #26485 ), #90369, .T. ) ;
#35396=ORIENTED_EDGE ( 'NONE', *, *, #42263, .T. ) ;
#35397=CARTESIAN_POINT ( 'NONE',  ( -66.52287095715007581, -23.47593901973090524, -1.443836447538997092 ) ) ;
#35398=CARTESIAN_POINT ( 'NONE',  ( -78.64728755545458228, -23.48783264082477018, -1.443836473390096797 ) ) ;
#35399=EDGE_CURVE ( 'NONE', #50327, #55686, #80362, .T. ) ;
#35403=CARTESIAN_POINT ( 'NONE',  ( -19.08498223313328168, 4.104482590468319536, 11.49999999999998934 ) ) ;
#35404=VECTOR ( 'NONE', #20560, 1000.000000000000114 ) ;
#35405=CARTESIAN_POINT ( 'NONE',  ( -2.751442626040462081, 21.25944542233241563, -1.500000000000002220 ) ) ;
#35409=CARTESIAN_POINT ( 'NONE',  ( 20.42703387425654427, 10.12935691860780985, -1.500000000000002220 ) ) ;
#35410=B_SPLINE_CURVE_WITH_KNOTS ( 'NONE', 3,
 ( #2929, #33859, #80531, #35856, #5405, #34365 ),
 .UNSPECIFIED., .F., .F.,
 ( 4, 2, 4 ),
 ( 0.000000000000000000, 0.001381509967656051590, 0.002763019935312103180 ),
 .UNSPECIFIED. ) ;
#35412=CARTESIAN_POINT ( 'NONE',  ( -129.5228709571500758, -29.50248528299804818, 1.056150453629047137 ) ) ;
#35414=CARTESIAN_POINT ( 'NONE',  ( 19.82558669001425500, -2.195561414069463702, 11.49999999999999645 ) ) ;
#35415=CARTESIAN_POINT ( 'NONE',  ( -31.52287095715006160, -23.72747288104469732, -1.053458166803228124 ) ) ;
#35416=CARTESIAN_POINT ( 'NONE',  ( -39.56088531193996261, -23.73791477778911130, 11.05961554403170943 ) ) ;
#35417=CARTESIAN_POINT ( 'NONE',  ( -48.49451331086643791, -24.34968618360933945, 0.1864209137778883862 ) ) ;
#35418=ORIENTED_EDGE ( 'NONE', *, *, #9937, .T. ) ;
#35420=CARTESIAN_POINT ( 'NONE',  ( -32.40344810634569939, -25.31516574674648368, 3.894478520810415567 ) ) ;
#35421=CARTESIAN_POINT ( 'NONE',  ( -13.51661872714272405, -17.00040112538478709, -1.500000000000002220 ) ) ;
#35423=CARTESIAN_POINT ( 'NONE',  ( -4.042178566331402045, 19.10766070095605684, -1.500000000000002220 ) ) ;
#35424=CARTESIAN_POINT ( 'NONE',  ( -55.56003084844635964, -23.85049219812686161, 10.88485053497527133 ) ) ;
#35427=CARTESIAN_POINT ( 'NONE',  ( -69.62287095715005592, -23.72773821059535848, 11.05748984161097503 ) ) ;
#35428=CARTESIAN_POINT ( 'NONE',  ( 6.539103723289373171, -19.38406401830294712, 11.49999999999999645 ) ) ;
#35430=DIRECTION ( 'NONE',  ( -3.773278334453079618E-23, 0.9999999999976377785, 2.173523156925979975E-06 ) ) ;
#35431=ORIENTED_EDGE ( 'NONE', *, *, #50928, .T. ) ;
#35432=FACE_OUTER_BOUND ( 'NONE', #18304, .T. ) ;
#35434=DIRECTION ( 'NONE',  ( 0.000000000000000000, 0.000000000000000000, 1.000000000000000000 ) ) ;
#35435=DIRECTION ( 'NONE',  ( 0.000000000000000000, 2.173523156925980399E-06, -0.9999999999976378895 ) ) ;
#35436=ORIENTED_EDGE ( 'NONE', *, *, #92176, .T. ) ;
#35439=CARTESIAN_POINT ( 'NONE',  ( 5.527175565732886042, -22.34193536506064603, 11.49999999999999645 ) ) ;
#35440=CARTESIAN_POINT ( 'NONE',  ( -17.61067154241388977, 14.45706175128816184, 11.49999999999998934 ) ) ;
#35441=CARTESIAN_POINT ( 'NONE',  ( -70.43669851199418019, -25.04371149268589392, 7.560212913825585801 ) ) ;
#35442=CARTESIAN_POINT ( 'NONE',  ( -28.62287095715006657, -24.50666107542846461, 1.056161637124864550 ) ) ;
#35444=CARTESIAN_POINT ( 'NONE',  ( -70.52287095715009002, -24.52232992886363050, 0.6492154411905990408 ) ) ;
#35445=CARTESIAN_POINT ( 'NONE',  ( -110.6324688656087432, -23.85016227208580375, -0.8807180028928308646 ) ) ;
#35446=CARTESIAN_POINT ( 'NONE',  ( -4.983756199382824548, -21.29032736245130053, -1.500000000000002220 ) ) ;
#35448=EDGE_CURVE ( 'NONE', #85219, #96161, #51260, .T. ) ;
#35451=CARTESIAN_POINT ( 'NONE',  ( -47.62287095715004881, -23.47593901973091235, -1.443836447539009749 ) ) ;
#35452=ORIENTED_EDGE ( 'NONE', *, *, #1812, .T. ) ;
#35454=CARTESIAN_POINT ( 'NONE',  ( -8.611577853089924517, -18.50786853157798006, -1.500000000000002220 ) ) ;
#35457=ORIENTED_EDGE ( 'NONE', *, *, #24913, .T. ) ;
#35458=VERTEX_POINT ( 'NONE', #73160 ) ;
#35459=CARTESIAN_POINT ( 'NONE',  ( 8.428894486204411507, 21.44871590506140890, 11.49999999999998934 ) ) ;
#35461=CARTESIAN_POINT ( 'NONE',  ( 8.473373031455752269, -18.34320851062214430, -1.500000000000002220 ) ) ;
#35463=PLANE ( 'NONE',  #16913 ) ;
#35464=EDGE_CURVE ( 'NONE', #37139, #96748, #45150, .T. ) ;
#35466=ADVANCED_FACE ( 'NONE', ( #65569 ), #20341, .F. ) ;
#35468=CARTESIAN_POINT ( 'NONE',  ( -41.62287095715006302, -23.95044443724991368, 10.65354141964650125 ) ) ;
#35469=CARTESIAN_POINT ( 'NONE',  ( 19.34736296927903254, -9.154118057783460216, 11.49999999999999645 ) ) ;
#35471=DIRECTION ( 'NONE',  ( 1.000000000000000000, 2.567145104884906770E-18, 5.579749332669698856E-24 ) ) ;
#35472=ADVANCED_FACE ( 'NONE', ( #26975 ), #14316, .T. ) ;
#35474=CARTESIAN_POINT ( 'NONE',  ( -16.22183044023116238, -15.26045173261249310, -1.500000000000002220 ) ) ;
#35475=CARTESIAN_POINT ( 'NONE',  ( -14.21563987850626276, 15.01860006206015008, 11.49999999999998934 ) ) ;
#35478=DIRECTION ( 'NONE',  ( 0.000000000000000000, 2.173523156925980399E-06, -0.9999999999976378895 ) ) ;
#35479=ORIENTED_EDGE ( 'NONE', *, *, #21004, .T. ) ;
#35480=PLANE ( 'NONE',  #75350 ) ;
#35483=CARTESIAN_POINT ( 'NONE',  ( -7.049398010371669798, 19.71092172866906012, -1.500000000000002220 ) ) ;
#35485=CARTESIAN_POINT ( 'NONE',  ( -9.857428550561325054, -19.57614489166009264, 11.49999999999999645 ) ) ;
#35486=CARTESIAN_POINT ( 'NONE',  ( -37.49075569243201755, -24.35071581493542325, 9.817618358456030592 ) ) ;
#35487=CARTESIAN_POINT ( 'NONE',  ( 9.939345090160914609, -20.19931669485651682, 11.49999999999998934 ) ) ;
#35488=CARTESIAN_POINT ( 'NONE',  ( 17.15856466979341377, 12.00972951212132855, 11.49999999999998934 ) ) ;
#35489=CARTESIAN_POINT ( 'NONE',  ( -85.52287095715006160, -29.50250243563736774, 8.947779886222139822 ) ) ;
#35491=CARTESIAN_POINT ( 'NONE',  ( -119.5565862188256148, -23.73791477778912551, 11.05961554403169878 ) ) ;
#35493=EDGE_CURVE ( 'NONE', #95501, #33464, #64580, .T. ) ;
#35494=ORIENTED_EDGE ( 'NONE', *, *, #16116, .T. ) ;
#35498=B_SPLINE_CURVE_WITH_KNOTS ( 'NONE', 3,
 ( #46221, #16270, #62456, #1056, #38607, #15765 ),
 .UNSPECIFIED., .F., .F.,
 ( 4, 2, 4 ),
 ( 0.000000000000000000, 0.001380764517854765182, 0.002761529035709530365 ),
 .UNSPECIFIED. ) ;
#35499=ADVANCED_FACE ( 'NONE', ( #54209 ), #59701, .T. ) ;
#35500=CARTESIAN_POINT ( 'NONE',  ( 19.78805588120126302, 8.271231038663975355, -1.500000000000002220 ) ) ;
#35503=CARTESIAN_POINT ( 'NONE',  ( 19.97611676871187569, -6.800378171449690257, 11.49999999999998934 ) ) ;
#35504=CARTESIAN_POINT ( 'NONE',  ( -100.0171587537243596, -25.20430878015014287, 3.360470424028859426 ) ) ;
#35505=AXIS2_PLACEMENT_3D ( 'NONE', #20083, #74373, #27709 ) ;
#35507=AXIS2_PLACEMENT_3D ( 'NONE', #38794, #91582, #69250 ) ;
#35508=CARTESIAN_POINT ( 'NONE',  ( -87.62287095715004170, -23.48783264082478794, -1.443836473390063269 ) ) ;
#35511=CARTESIAN_POINT ( 'NONE',  ( -4.445301477617020325, 21.63612927058290936, -1.500000000000002220 ) ) ;
#35514=CARTESIAN_POINT ( 'NONE',  ( -60.53049054233731852, -24.92564183028978775, 1.928384488918253092 ) ) ;
#35515=AXIS2_PLACEMENT_3D ( 'NONE', #59814, #29342, #82626 ) ;
#35516=ADVANCED_FACE ( 'NONE', ( #59940 ), #10097, .T. ) ;
#35517=CARTESIAN_POINT ( 'NONE',  ( -62.59277029813154059, -24.15620529776627379, 10.23563542870660825 ) ) ;
#35518=ORIENTED_EDGE ( 'NONE', *, *, #59283, .F. ) ;
#35521=CARTESIAN_POINT ( 'NONE',  ( -9.778911232092227124, -18.99720643767551209, 11.49999999999998934 ) ) ;
#35522=CARTESIAN_POINT ( 'NONE',  ( -70.34543693012690824, -25.04307398257883577, 7.563174194274490780 ) ) ;
#35523=CARTESIAN_POINT ( 'NONE',  ( -49.88527226319177288, -25.31392319263090585, 5.203681702801227438 ) ) ;
#35527=CARTESIAN_POINT ( 'NONE',  ( 3.867644355387967359, 22.30990608135428488, -1.500000000000002220 ) ) ;
#35528=CARTESIAN_POINT ( 'NONE',  ( -47.52287095715006870, -23.96127896942173763, -0.6493128930931011400 ) ) ;
#35530=CARTESIAN_POINT ( 'NONE',  ( -50.65946795233809041, -25.31358068923536564, 5.223679172549864802 ) ) ;
#35531=LINE ( 'NONE', #50255, #34643 ) ;
#35532=CARTESIAN_POINT ( 'NONE',  ( 19.26447527235507451, 4.322997736827044690, 11.49999999999999645 ) ) ;
#35533=DIRECTION ( 'NONE',  ( -3.773278334444166432E-23, 1.000000000000000000, 0.000000000000000000 ) ) ;
#35535=CARTESIAN_POINT ( 'NONE',  ( -67.54436619133976194, -24.34968618360932879, 0.1864209137778810865 ) ) ;
#35538=PLANE ( 'NONE',  #23777 ) ;
#35539=CARTESIAN_POINT ( 'NONE',  ( -100.7619115510279926, -25.12268558752044001, 7.069363477253397754 ) ) ;
#35540=CARTESIAN_POINT ( 'NONE',  ( 2.319523670979641849, -21.48760272935114557, -1.500000000000002220 ) ) ;
#35541=CARTESIAN_POINT ( 'NONE',  ( -98.52287095715006160, -29.50247984919015209, -1.443849546365050029 ) ) ;
#35542=CARTESIAN_POINT ( 'NONE',  ( -66.52287095715006160, -23.48786465467241769, 11.44779295918254647 ) ) ;
#35543=CARTESIAN_POINT ( 'NONE',  ( -109.5562042904833930, -23.47593901973091235, -1.443836447538999312 ) ) ;
#35545=CARTESIAN_POINT ( 'NONE',  ( -18.77405512783484198, 6.205181830411797606, 11.49999999999998934 ) ) ;
#35546=VERTEX_POINT ( 'NONE', #64337 ) ;
#35547=CARTESIAN_POINT ( 'NONE',  ( 20.05935882324986963, -3.104462954613115500, 11.49999999999999645 ) ) ;
#35549=AXIS2_PLACEMENT_3D ( 'NONE', #7190, #15302, #31032 ) ;
#35552=B_SPLINE_SURFACE_WITH_KNOTS ( 'NONE', 3, 3, ( 
 ( #96069, #32158, #71235, #78818 ),
 ( #2731, #1722, #10328, #26563 ),
 ( #63637, #64144, #41797, #79830 ),
 ( #40776, #94558, #25552, #72740 ),
 ( #86450, #72237, #8829, #95564 ),
 ( #9826, #56521, #39766, #71738 ),
 ( #33668, #64649, #70728, #1224 ),
 ( #26048, #63131, #94057, #24543 ),
 ( #57021, #55516, #41281, #9314 ),
 ( #87959, #40280, #18438, #32660 ) ),
 .UNSPECIFIED., .F., .F., .F.,
 ( 4, 3, 3, 4 ),
 ( 4, 4 ),
 ( 0.7022005934544808259, 0.7765311282028797280, 0.8508616629512786300, 0.9995227324480764342 ),
 ( 0.5495603210497661539, 0.5509005761542268287 ),
 .UNSPECIFIED. ) ;
#35553=DIRECTION ( 'NONE',  ( 3.773278334444167608E-23, -1.000000000000000000, 0.000000000000000000 ) ) ;
#35554=CARTESIAN_POINT ( 'NONE',  ( -107.5228709571500758, -23.47596703998600631, 11.44779298504228038 ) ) ;
#35555=DIRECTION ( 'NONE',  ( -3.773278334453079030E-23, 0.9999999999976377785, 2.173523156925979128E-06 ) ) ;
#35556=CARTESIAN_POINT ( 'NONE',  ( -45.62287095715004881, -29.50247984919015209, -1.443849546365058689 ) ) ;
#35557=CARTESIAN_POINT ( 'NONE',  ( -51.52472467211992324, -25.24108473429059885, 6.254983020916855097 ) ) ;
#35558=CARTESIAN_POINT ( 'NONE',  ( 9.011679573027636891, 17.89655708981447901, -1.500000000000002220 ) ) ;
#35561=B_SPLINE_CURVE_WITH_KNOTS ( 'NONE', 3,
 ( #59984, #28028, #44256, #12784, #74688, #75677 ),
 .UNSPECIFIED., .F., .F.,
 ( 4, 2, 4 ),
 ( 6.391158118967745954E-06, 0.001387004593080785496, 0.002767618028042603297 ),
 .UNSPECIFIED. ) ;
#35562=CARTESIAN_POINT ( 'NONE',  ( -32.62287095715004881, -23.48786465467240347, 11.44779295918255535 ) ) ;
#35563=CARTESIAN_POINT ( 'NONE',  ( -115.5228709571500616, -23.48783264082477018, -1.443836473390083475 ) ) ;
#35565=LINE ( 'NONE', #33560, #15669 ) ;
#35566=LINE ( 'NONE', #68016, #26763 ) ;
#35567=CARTESIAN_POINT ( 'NONE',  ( -71.55620429048339304, -24.66019654487199375, 8.947790411086131712 ) ) ;
#35568=VERTEX_POINT ( 'NONE', #96751 ) ;
#35570=CARTESIAN_POINT ( 'NONE',  ( 16.70477854660759931, 11.60849435585976153, 11.49999999999998934 ) ) ;
#35572=EDGE_CURVE ( 'NONE', #65047, #24849, #80527, .T. ) ;
#35573=CARTESIAN_POINT ( 'NONE',  ( 19.00551534866085746, 12.86435971046890359, 11.49999999999998934 ) ) ;
#35574=CARTESIAN_POINT ( 'NONE',  ( -32.58048861069256930, -24.51314013834315375, 0.6176544820404111791 ) ) ;
#35575=EDGE_CURVE ( 'NONE', #4586, #97579, #19792, .T. ) ;
#35576=ORIENTED_EDGE ( 'NONE', *, *, #67090, .F. ) ;
#35578=CARTESIAN_POINT ( 'NONE',  ( -49.41394411914537699, -25.30232982750377246, 4.714210424874468508 ) ) ;
#35580=CARTESIAN_POINT ( 'NONE',  ( -49.27764846858840997, -25.12215211752863198, 6.145205272392983531 ) ) ;
#35583=CARTESIAN_POINT ( 'NONE',  ( 18.66760434907605060, -10.05535386721697222, 11.49999999999999645 ) ) ;
#35585=ORIENTED_EDGE ( 'NONE', *, *, #71554, .F. ) ;
#35586=CARTESIAN_POINT ( 'NONE',  ( -12.04397493737346991, 18.63154960201688226, 11.49999999999998934 ) ) ;
#35587=CARTESIAN_POINT ( 'NONE',  ( 20.22723401096548201, -3.897675682603606084, 11.49999999999998934 ) ) ;
#35591=CARTESIAN_POINT ( 'NONE',  ( -61.52287095715006160, -23.47596703998600631, 11.44779298504228926 ) ) ;
#35593=CARTESIAN_POINT ( 'NONE',  ( -113.6228709571500559, -29.50250243563736774, 8.947779886222136270 ) ) ;
#35594=ORIENTED_EDGE ( 'NONE', *, *, #77743, .T. ) ;
#35595=ORIENTED_EDGE ( 'NONE', *, *, #88958, .F. ) ;
#35599=CARTESIAN_POINT ( 'NONE',  ( -28.62169072633495404, -23.33141450733164390, 11.44779300624183982 ) ) ;
#35600=CARTESIAN_POINT ( 'NONE',  ( -119.5562042904834072, -23.48783264082478794, -1.443836473390058384 ) ) ;
#35601=CARTESIAN_POINT ( 'NONE',  ( 12.20387445076365296, 16.77033177596414504, -1.500000000000002220 ) ) ;
#35602=CARTESIAN_POINT ( 'NONE',  ( 18.07971092720299922, 12.08445254275838465, 11.49999999999999645 ) ) ;
#35603=ORIENTED_EDGE ( 'NONE', *, *, #71265, .F. ) ;
#35604=CARTESIAN_POINT ( 'NONE',  ( -121.6228709571500417, -23.47593901973091235, -1.443836447538997536 ) ) ;
#35605=CARTESIAN_POINT ( 'NONE',  ( -115.5550176680797847, -24.15503026093914940, -0.2815557561904543094 ) ) ;
#35606=CARTESIAN_POINT ( 'NONE',  ( -21.67104271438225638, 5.786422744429515319, 11.49999999999998934 ) ) ;
#35608=CARTESIAN_POINT ( 'NONE',  ( -65.49048155462992327, -24.73486907724918282, 1.287355809206962354 ) ) ;
#35609=ORIENTED_EDGE ( 'NONE', *, *, #68826, .T. ) ;
#35611=CARTESIAN_POINT ( 'NONE',  ( -38.62287095715005592, -29.50250243563736774, 8.947779886222148704 ) ) ;
#35612=ORIENTED_EDGE ( 'NONE', *, *, #49113, .T. ) ;
#35616=CARTESIAN_POINT ( 'NONE',  ( 21.17668642892995834, 2.279540523802085605, -1.500000000000002220 ) ) ;
#35617=VERTEX_POINT ( 'NONE', #57219 ) ;
#35618=CARTESIAN_POINT ( 'NONE',  ( -88.58338540734003175, -24.65952944569304606, 1.056160979905700126 ) ) ;
#35619=CARTESIAN_POINT ( 'NONE',  ( 9.643594380127815668, 19.59848315111488759, 11.49999999999998934 ) ) ;
#35620=CARTESIAN_POINT ( 'NONE',  ( -124.5228709571500616, -23.47596703998600631, 11.44779298504227860 ) ) ;
#35621=CARTESIAN_POINT ( 'NONE',  ( 7.379361219544559702, 21.46082085352547963, -1.500000000000002220 ) ) ;
#35622=CARTESIAN_POINT ( 'NONE',  ( -41.01720553446741491, -25.28892453938848561, 3.440463365724605982 ) ) ;
#35624=CARTESIAN_POINT ( 'NONE',  ( 21.83198049998918577, 2.282343850347359648, -1.500000000000002220 ) ) ;
#35626=VERTEX_POINT ( 'NONE', #88651 ) ;
#35627=CARTESIAN_POINT ( 'NONE',  ( -122.6256518724121349, -23.96169478059714564, 10.65365249895717170 ) ) ;
#35628=CARTESIAN_POINT ( 'NONE',  ( -49.13273521788515552, -25.26337483015602814, 6.968846308470279638 ) ) ;
#35629=EDGE_CURVE ( 'NONE', #27877, #61563, #3988, .T. ) ;
#35631=CARTESIAN_POINT ( 'NONE',  ( -30.59802378171020720, -24.75939178235423910, 8.616593176194657033 ) ) ;
#35633=CARTESIAN_POINT ( 'NONE',  ( -20.38992538795168130, -24.51867817427762120, 3.856996771330998719 ) ) ;
#35634=CARTESIAN_POINT ( 'NONE',  ( 1.567330217057175901, -21.20382687294985047, 11.49999999999998934 ) ) ;
#35635=CARTESIAN_POINT ( 'NONE',  ( -112.5515245461530469, -24.51314013834317151, 0.6176544820404297198 ) ) ;
#35636=CARTESIAN_POINT ( 'NONE',  ( -26.17837527425876942, -24.75186326096774536, 3.912474607469140775 ) ) ;
#35639=CARTESIAN_POINT ( 'NONE',  ( -85.58384127135377639, -24.83618233451450408, 1.606449574219535270 ) ) ;
#35640=CARTESIAN_POINT ( 'NONE',  ( -129.5228709571501327, -23.96127896941634106, -0.6493128931037915885 ) ) ;
#35641=CARTESIAN_POINT ( 'NONE',  ( -32.55620429048338593, -23.47593901973091235, -1.443836447539013301 ) ) ;
#35642=ORIENTED_EDGE ( 'NONE', *, *, #65306, .F. ) ;
#35643=CARTESIAN_POINT ( 'NONE',  ( 17.64699390344983598, -8.409456921668478913, 11.49999999999999645 ) ) ;
#35646=CARTESIAN_POINT ( 'NONE',  ( -79.35273227324233858, -25.25510918649008829, 6.111704383075113434 ) ) ;
#35647=ORIENTED_EDGE ( 'NONE', *, *, #35572, .F. ) ;
#35649=CARTESIAN_POINT ( 'NONE',  ( -101.3289322354959836, -25.08272168729980223, 7.323006979996904420 ) ) ;
#35650=VECTOR ( 'NONE', #42381, 1000.000000000000114 ) ;
#35651=CARTESIAN_POINT ( 'NONE',  ( -42.58953762381671737, -23.48783264082477373, -1.443836473390072817 ) ) ;
#35653=CARTESIAN_POINT ( 'NONE',  ( 16.13486940644654766, 11.28601765141728741, -1.500000000000002220 ) ) ;
#35654=AXIS2_PLACEMENT_3D ( 'NONE', #55935, #41204, #64563 ) ;
#35657=LINE ( 'NONE', #97543, #32664 ) ;
#35662=CARTESIAN_POINT ( 'NONE',  ( -107.5895376238167387, -24.64965694238407679, 8.947790433994649462 ) ) ;
#35663=CARTESIAN_POINT ( 'NONE',  ( -45.62287095715005592, -24.63345952396255711, 9.038047939301497635 ) ) ;
#35664=CARTESIAN_POINT ( 'NONE',  ( -123.6228709571500559, -29.50250786944525672, 11.44777988621622811 ) ) ;
#35665=FACE_OUTER_BOUND ( 'NONE', #72174, .T. ) ;
#35666=CARTESIAN_POINT ( 'NONE',  ( -89.52287095715006160, -23.48786465467241769, 11.44779295918254292 ) ) ;
#35667=CARTESIAN_POINT ( 'NONE',  ( -70.35895856474228083, -25.31201590484430142, 5.313173609717679824 ) ) ;
#35668=CARTESIAN_POINT ( 'NONE',  ( -107.5907586917641083, -24.15543982623907837, -0.2315651400026443874 ) ) ;
#35669=CARTESIAN_POINT ( 'NONE',  ( -4.495603250223349612, -19.44740727768710187, -1.500000000000002220 ) ) ;
#35671=CARTESIAN_POINT ( 'NONE',  ( -0.03708603945156426634, -22.56989207558077126, 1.621508199058790511 ) ) ;
#35673=CARTESIAN_POINT ( 'NONE',  ( -63.52287095715007581, -24.50216790748205042, 0.6166512839542489521 ) ) ;
#35675=EDGE_CURVE ( 'NONE', #18738, #87632, #42491, .T. ) ;
#35677=CARTESIAN_POINT ( 'NONE',  ( -126.1689479211560183, -25.21288074133898505, 6.500980345380262371 ) ) ;
#35678=PLANE ( 'NONE',  #19228 ) ;
#35679=CARTESIAN_POINT ( 'NONE',  ( -64.52287095715006160, -24.65952944569304606, 1.056160979905695463 ) ) ;
#35682=DIRECTION ( 'NONE',  ( -1.000000000000000000, -3.773278334444167608E-23, -8.201307833595939069E-29 ) ) ;
#35684=ORIENTED_EDGE ( 'NONE', *, *, #21233, .F. ) ;
#35685=EDGE_CURVE ( 'NONE', #77233, #98717, #11351, .T. ) ;
#35686=CARTESIAN_POINT ( 'NONE',  ( -2.479824388263708990, 20.08073137130260122, -1.500000000000002220 ) ) ;
#35687=CARTESIAN_POINT ( 'NONE',  ( -43.55620429048337883, -23.48783264082477373, -1.443836473390070596 ) ) ;
#35690=CARTESIAN_POINT ( 'NONE',  ( -50.62287095715005592, -29.50250786944525672, 11.44777988621624054 ) ) ;
#35691=ADVANCED_FACE ( 'NONE', ( #48602 ), #79525, .T. ) ;
#35693=CARTESIAN_POINT ( 'NONE',  ( -46.62287095715004881, -24.64965695001467694, 8.947790433994185832 ) ) ;
#35694=CARTESIAN_POINT ( 'NONE',  ( -52.52287095715009002, -24.51387760970726148, 9.387446482453432495 ) ) ;
#35695=CARTESIAN_POINT ( 'NONE',  ( 19.65109224456760728, -3.968444974485820786, -1.500000000000002220 ) ) ;
#35696=EDGE_CURVE ( 'NONE', #17632, #12369, #54854, .T. ) ;
#35697=CARTESIAN_POINT ( 'NONE',  ( 4.297136154115697160, 20.59472113332480703, 11.49999999999999645 ) ) ;
#35699=CARTESIAN_POINT ( 'NONE',  ( -111.6228709571500843, -23.47596703998600631, 11.44779298504227860 ) ) ;
#35700=CARTESIAN_POINT ( 'NONE',  ( -7.692412698405892257, 20.70400481474656118, 11.49999999999998934 ) ) ;
#35703=CARTESIAN_POINT ( 'NONE',  ( -40.31138024738270786, -25.27806106079862403, 5.079523691001327279 ) ) ;
#35704=CARTESIAN_POINT ( 'NONE',  ( -76.62287095715007013, -23.47593901973091235, -1.443836447539004642 ) ) ;
#35707=DIRECTION ( 'NONE',  ( -3.773278334453080206E-23, 0.9999999999976377785, 2.173523156925979975E-06 ) ) ;
#35709=CARTESIAN_POINT ( 'NONE',  ( -31.62287095715005947, -23.96127896941631619, -0.6493128931037948082 ) ) ;
#35710=ORIENTED_EDGE ( 'NONE', *, *, #100353, .T. ) ;
#35711=EDGE_LOOP ( 'NONE', ( #27152, #92033, #35045, #44585, #70280, #77199 ) ) ;
#35712=CARTESIAN_POINT ( 'NONE',  ( -43.52287095715006160, -23.47596703998600631, 11.44779298504229281 ) ) ;
#35714=CARTESIAN_POINT ( 'NONE',  ( -76.59214954560788158, -24.15543982623907482, -0.2315651400026599305 ) ) ;
#35715=EDGE_CURVE ( 'NONE', #46190, #78417, #57397, .T. ) ;
#35716=CARTESIAN_POINT ( 'NONE',  ( 4.697267095454844998, -20.06606415395816967, -1.500000000000002220 ) ) ;
#35717=CARTESIAN_POINT ( 'NONE',  ( -19.35566633068252074, -9.524217769563914970, 11.49999999999999645 ) ) ;
#35718=VERTEX_POINT ( 'NONE', #90139 ) ;
#35719=CARTESIAN_POINT ( 'NONE',  ( -91.63415237563449978, -23.96119346886881019, -0.6495511937832073590 ) ) ;
#35720=DIRECTION ( 'NONE',  ( 3.773278334444167608E-23, -1.000000000000000000, 0.000000000000000000 ) ) ;
#35721=PLANE ( 'NONE',  #93381 ) ;
#35722=CARTESIAN_POINT ( 'NONE',  ( 18.00092565640838416, -13.26076702590692769, -1.500000000000002220 ) ) ;
#35723=CARTESIAN_POINT ( 'NONE',  ( -59.62287095715007013, -23.73934037231756733, 11.05740245334329153 ) ) ;
#35725=EDGE_LOOP ( 'NONE', ( #37734, #40924, #55470, #5492 ) ) ;
#35728=CARTESIAN_POINT ( 'NONE',  ( -51.37905358277658507, -25.30232438542244466, 4.713790514697788758 ) ) ;
#35730=CARTESIAN_POINT ( 'NONE',  ( -11.44352472427880052, 17.46665840655709090, -1.500000000000002220 ) ) ;
#35732=CARTESIAN_POINT ( 'NONE',  ( -39.98807537358911190, -25.12223002584979881, 2.898744922101010424 ) ) ;
#35735=VECTOR ( 'NONE', #42026, 1000.000000000000114 ) ;
#35736=CARTESIAN_POINT ( 'NONE',  ( -100.5143450367917808, -24.15602025860896163, 10.28564288303535790 ) ) ;
#35737=CARTESIAN_POINT ( 'NONE',  ( -20.28541985502614509, -5.886007371444655689, -1.500000000000002220 ) ) ;
#35740=CARTESIAN_POINT ( 'NONE',  ( -91.55620429048339304, -24.66019654487199375, 8.947790411086124607 ) ) ;
#35741=CARTESIAN_POINT ( 'NONE',  ( -58.52287095715004739, -23.48783264082477018, -1.443836473390092801 ) ) ;
#35742=CARTESIAN_POINT ( 'NONE',  ( -117.6228709571500559, -29.50250243563736774, 8.947779886222134493 ) ) ;
#35743=CARTESIAN_POINT ( 'NONE',  ( -28.55620429048340370, -23.31439381047619008, -1.443835771460519890 ) ) ;
#35745=CARTESIAN_POINT ( 'NONE',  ( 9.899741330608472722, -19.37759744025533593, -1.500000000000002220 ) ) ;
#35747=CARTESIAN_POINT ( 'NONE',  ( 13.23790625878087468, -17.95846084735695314, 11.49999999999999645 ) ) ;
#35748=ORIENTED_EDGE ( 'NONE', *, *, #95135, .T. ) ;
#35752=DIRECTION ( 'NONE',  ( -0.000000000000000000, 2.173523156925979552E-06, -0.9999999999976378895 ) ) ;
#35754=CARTESIAN_POINT ( 'NONE',  ( -54.62287095715005592, -24.66019654487199020, 8.947790411086135265 ) ) ;
#35755=ORIENTED_EDGE ( 'NONE', *, *, #85977, .T. ) ;
#35756=EDGE_CURVE ( 'NONE', #35375, #53340, #16201, .T. ) ;
#35757=ORIENTED_EDGE ( 'NONE', *, *, #72821, .F. ) ;
#35759=CARTESIAN_POINT ( 'NONE',  ( -86.62287095715001328, -23.47596703998600631, 11.44779298504227683 ) ) ;
#35760=CARTESIAN_POINT ( 'NONE',  ( -90.52287095715006160, -29.50247984919015209, -1.443849546365051806 ) ) ;
#35761=CARTESIAN_POINT ( 'NONE',  ( -35.52287095715009713, -24.51163499207175889, 0.6490370598554275894 ) ) ;
#35765=CARTESIAN_POINT ( 'NONE',  ( -17.02366064725396555, -9.230830265533395362, 11.49999999999999645 ) ) ;
#35766=CARTESIAN_POINT ( 'NONE',  ( -88.52287095715006160, -23.47596703998600631, 11.44779298504228393 ) ) ;
#35767=EDGE_CURVE ( 'NONE', #89034, #33339, #6507, .T. ) ;
#35772=CARTESIAN_POINT ( 'NONE',  ( -30.61342099046267862, -24.26827793580485704, 9.960784317162946877 ) ) ;
#35773=CARTESIAN_POINT ( 'NONE',  ( -15.04504930077994196, -12.58455232801425794, 11.49999999999998934 ) ) ;
#35774=CARTESIAN_POINT ( 'NONE',  ( -116.5895376238167103, -24.65952944569305316, 1.056160979905705455 ) ) ;
#35775=ORIENTED_EDGE ( 'NONE', *, *, #91797, .T. ) ;
#35776=CARTESIAN_POINT ( 'NONE',  ( 4.073501596442082651, -21.17334570714589859, 11.49999999999998934 ) ) ;
#35777=CARTESIAN_POINT ( 'NONE',  ( -37.62287095715005592, -23.47593901973091235, -1.443836447539011525 ) ) ;
#35778=CARTESIAN_POINT ( 'NONE',  ( -81.37613735670856840, -25.31572692185423534, 5.179459861000572651 ) ) ;
#35781=FACE_OUTER_BOUND ( 'NONE', #40185, .T. ) ;
#35782=CARTESIAN_POINT ( 'NONE',  ( -2.116611060711651504, 22.89395876494169002, -1.500000000000002220 ) ) ;
#35786=CARTESIAN_POINT ( 'NONE',  ( -16.67386609800740516, 11.36076560755915033, 11.49999999999999645 ) ) ;
#35787=CARTESIAN_POINT ( 'NONE',  ( -108.9559085688801616, -25.10927677356297139, 4.125626278649611400 ) ) ;
#35790=FACE_OUTER_BOUND ( 'NONE', #54096, .T. ) ;
#35791=LINE ( 'NONE', #72361, #86698 ) ;
#35792=CARTESIAN_POINT ( 'NONE',  ( 10.41257876278241845, -16.90412932818451353, -1.500000000000002220 ) ) ;
#35793=CARTESIAN_POINT ( 'NONE',  ( -113.5881261692640152, -24.51314013834316086, 0.6176544820404182845 ) ) ;
#35794=CARTESIAN_POINT ( 'NONE',  ( 19.18734209777730015, 4.435579877058994036, -1.500000000000002220 ) ) ;
#35795=CARTESIAN_POINT ( 'NONE',  ( -42.48688622151200178, -24.51314013834315375, 0.6176544820404090697 ) ) ;
#35796=AXIS2_PLACEMENT_3D ( 'NONE', #56062, #72784, #64188 ) ;
#35798=CARTESIAN_POINT ( 'NONE',  ( -100.5228709571500616, -23.48786465467242479, 11.44779295918254114 ) ) ;
#35799=CARTESIAN_POINT ( 'NONE',  ( 3.034461355793923509, -20.43525710956717845, 11.49999999999999645 ) ) ;
#35802=B_SPLINE_CURVE_WITH_KNOTS ( 'NONE', 3,
 ( #66072, #98472, #75633, #20851, #21844, #91369 ),
 .UNSPECIFIED., .F., .F.,
 ( 4, 2, 4 ),
 ( 0.000000000000000000, 0.001380764517854759978, 0.002761529035709519957 ),
 .UNSPECIFIED. ) ;
#35803=CARTESIAN_POINT ( 'NONE',  ( -22.46375958613465684, 3.124547546656453179, 11.49999999999999645 ) ) ;
#35808=CARTESIAN_POINT ( 'NONE',  ( -63.59779725530248840, -23.96119346886879953, -0.6495511937832106897 ) ) ;
#35809=CARTESIAN_POINT ( 'NONE',  ( -45.52287095715006160, -25.00158670708908915, 2.256160236439166411 ) ) ;
#35810=EDGE_LOOP ( 'NONE', ( #50181, #97802, #42366, #92592 ) ) ;
#35811=ORIENTED_EDGE ( 'NONE', *, *, #46594, .T. ) ;
#35812=CARTESIAN_POINT ( 'NONE',  ( -44.62287095715004881, -29.50247984919015209, -1.443849546365060466 ) ) ;
#35813=CARTESIAN_POINT ( 'NONE',  ( 4.181975289622855918, -22.47981636197143374, -1.500000000000002220 ) ) ;
#35814=CARTESIAN_POINT ( 'NONE',  ( -29.57133676521425514, -23.40473823521239183, -1.443836171194816886 ) ) ;
#35815=CARTESIAN_POINT ( 'NONE',  ( 7.401388779597747103, 20.28278527911644247, -1.500000000000002220 ) ) ;
#35816=CARTESIAN_POINT ( 'NONE',  ( -113.5164963221879901, -24.35071581493543746, 9.817618358456018157 ) ) ;
#35818=EDGE_CURVE ( 'NONE', #40297, #39807, #5401, .T. ) ;
#35819=CARTESIAN_POINT ( 'NONE',  ( -11.58057713800463162, -19.31455136971746001, 11.49999999999999645 ) ) ;
#35821=CARTESIAN_POINT ( 'NONE',  ( -69.64187497903644442, -25.24754278231193894, 5.000677553795553898 ) ) ;
#35822=CARTESIAN_POINT ( 'NONE',  ( -10.95654650054425794, 19.06054500580150446, -1.500000000000002220 ) ) ;
#35824=CARTESIAN_POINT ( 'NONE',  ( -44.66289782833593591, -23.48786465467240347, 11.44779295918255180 ) ) ;
#35828=PLANE ( 'NONE',  #34892 ) ;
#35829=ORIENTED_EDGE ( 'NONE', *, *, #94445, .F. ) ;
#35830=DIRECTION ( 'NONE',  ( -3.773278334444166432E-23, 1.000000000000000000, 0.000000000000000000 ) ) ;
#35833=CARTESIAN_POINT ( 'NONE',  ( -65.52287095715007581, -24.51163499207173402, 0.6490370598554309201 ) ) ;
#35834=LINE ( 'NONE', #4396, #82703 ) ;
#35835=CARTESIAN_POINT ( 'NONE',  ( -57.51496554766011826, -23.73766607897670866, -1.055555164236458454 ) ) ;
#35836=ADVANCED_FACE ( 'NONE', ( #67309 ), #35365, .F. ) ;
#35837=CARTESIAN_POINT ( 'NONE',  ( -16.87313589883980214, -11.49665204554024989, -1.500000000000002220 ) ) ;
#35838=ORIENTED_EDGE ( 'NONE', *, *, #78118, .T. ) ;
#35839=CARTESIAN_POINT ( 'NONE',  ( -70.78845123859034061, -25.04713129051003051, 7.496186878019077682 ) ) ;
#35840=CARTESIAN_POINT ( 'NONE',  ( -115.6228709571500417, -24.62285846362215835, 9.038163152653526211 ) ) ;
#35841=CARTESIAN_POINT ( 'NONE',  ( -105.6235594576710781, -25.00158670708910691, 2.256160236439218369 ) ) ;
#35842=CARTESIAN_POINT ( 'NONE',  ( -63.52287095715006160, -23.47596703998600631, 11.44779298504228926 ) ) ;
#35843=ORIENTED_EDGE ( 'NONE', *, *, #15745, .F. ) ;
#35847=CARTESIAN_POINT ( 'NONE',  ( 5.792680761630559338, -19.98616098212858105, 11.49999999999998934 ) ) ;
#35849=ORIENTED_EDGE ( 'NONE', *, *, #54936, .T. ) ;
#35850=CARTESIAN_POINT ( 'NONE',  ( -39.47626860353659595, -25.29241910976760366, 4.433561829988058811 ) ) ;
#35853=CARTESIAN_POINT ( 'NONE',  ( -54.52287095715006870, -24.64898659630367916, 1.056161002820821038 ) ) ;
#35855=VERTEX_POINT ( 'NONE', #21605 ) ;
#35856=CARTESIAN_POINT ( 'NONE',  ( -29.62287095715005236, -24.26166599405031121, 0.1849422882210577934 ) ) ;
#35857=B_SPLINE_CURVE_WITH_KNOTS ( 'NONE', 3,
 ( #55743, #80557, #26774, #86669 ),
 .UNSPECIFIED., .F., .F.,
 ( 4, 4 ),
 ( 0.7993502183265108751, 0.8003509653672765678 ),
 .UNSPECIFIED. ) ;
#35858=CARTESIAN_POINT ( 'NONE',  ( -64.52287095715010423, -24.66019654487200441, 8.947790411086119278 ) ) ;
#35859=B_SPLINE_CURVE_WITH_KNOTS ( 'NONE', 3,
 ( #50804, #27467, #66049, #51801, #96466, #13214 ),
 .UNSPECIFIED., .F., .F.,
 ( 4, 2, 4 ),
 ( 0.000000000000000000, 0.001380764517853247733, 0.002761529035706495466 ),
 .UNSPECIFIED. ) ;
#35861=FACE_OUTER_BOUND ( 'NONE', #4623, .T. ) ;
#35862=CARTESIAN_POINT ( 'NONE',  ( 20.57837473233041692, -7.934362236255416256, 11.49999999999999645 ) ) ;
#35864=CARTESIAN_POINT ( 'NONE',  ( -108.5876547150312206, -24.51314013834316086, 0.6176544820404235026 ) ) ;
#35865=CARTESIAN_POINT ( 'NONE',  ( 8.141615846073909424, -21.09679883994429161, 11.49999999999998934 ) ) ;
#35866=CARTESIAN_POINT ( 'NONE',  ( -115.5535801380732295, -24.40133493613050675, 9.663955038902797057 ) ) ;
#35867=EDGE_LOOP ( 'NONE', ( #72903, #85806, #70410, #23434 ) ) ;
#35868=EDGE_CURVE ( 'NONE', #68025, #57950, #52576, .T. ) ;
#35870=ORIENTED_EDGE ( 'NONE', *, *, #43126, .F. ) ;
#35873=ADVANCED_FACE ( 'NONE', ( #82027 ), #49006, .T. ) ;
#35875=CARTESIAN_POINT ( 'NONE',  ( -57.59851968582830040, -23.96169478059713143, 10.65365249895718058 ) ) ;
#35878=CARTESIAN_POINT ( 'NONE',  ( -7.755428854246955161, -20.87388092083558888, -1.500000000000002220 ) ) ;
#35879=LINE ( 'NONE', #66849, #27390 ) ;
#35880=ORIENTED_EDGE ( 'NONE', *, *, #40223, .F. ) ;
#35881=CARTESIAN_POINT ( 'NONE',  ( -120.5228709571500616, -24.99132157543167310, 2.256160258750667502 ) ) ;
#35882=CARTESIAN_POINT ( 'NONE',  ( -37.53291846491953976, -24.51314013834316796, 0.6176544820404176184 ) ) ;
#35883=CARTESIAN_POINT ( 'NONE',  ( -108.6228709571500275, -24.51283580621365132, 0.6167428607019852516 ) ) ;
#35884=CARTESIAN_POINT ( 'NONE',  ( -49.55620429048339304, -24.66019654487199020, 8.947790411086135265 ) ) ;
#35885=CARTESIAN_POINT ( 'NONE',  ( -19.34354882100874562, 2.624169249526263403, -1.500000000000002220 ) ) ;
#35886=CARTESIAN_POINT ( 'NONE',  ( -11.90495014755217618, 17.82271480561356469, 11.49999999999998934 ) ) ;
#35887=B_SPLINE_CURVE_WITH_KNOTS ( 'NONE', 3,
 ( #60360, #35997, #97886, #28382, #13648, #67964 ),
 .UNSPECIFIED., .F., .F.,
 ( 4, 2, 4 ),
 ( 0.000000000000000000, 0.001380901958385389412, 0.002761803916770778824 ),
 .UNSPECIFIED. ) ;
#35889=FACE_OUTER_BOUND ( 'NONE', #66691, .T. ) ;
#35891=CARTESIAN_POINT ( 'NONE',  ( -15.22011711465338912, -17.00649957279452451, -1.500000000000002220 ) ) ;
#35896=CARTESIAN_POINT ( 'NONE',  ( 10.22567584263966722, 17.17405255344276682, 11.49999999999999645 ) ) ;
#35897=FACE_OUTER_BOUND ( 'NONE', #22465, .T. ) ;
#35898=DIRECTION ( 'NONE',  ( -3.773278334444167608E-23, 1.000000000000000000, 0.000000000000000000 ) ) ;
#35899=CARTESIAN_POINT ( 'NONE',  ( -48.50692445814570419, -23.96119346886881019, -0.6495511937831938143 ) ) ;
#35901=CARTESIAN_POINT ( 'NONE',  ( -112.6228709571500559, -29.50250786944525672, 11.44777988621622988 ) ) ;
#35903=CARTESIAN_POINT ( 'NONE',  ( -14.78470843206283902, -15.91074852019131924, 11.49999999999998934 ) ) ;
#35904=EDGE_CURVE ( 'NONE', #87999, #50459, #76879, .T. ) ;
#35906=CARTESIAN_POINT ( 'NONE',  ( -12.10551386448753064, 15.32171617432465816, -1.500000000000002220 ) ) ;
#35907=EDGE_CURVE ( 'NONE', #14750, #96384, #81446, .T. ) ;
#35909=B_SPLINE_CURVE_WITH_KNOTS ( 'NONE', 3,
 ( #90853, #12717, #97468, #5117 ),
 .UNSPECIFIED., .F., .F.,
 ( 4, 4 ),
 ( 0.000000000000000000, 9.999999999998206125E-05 ),
 .UNSPECIFIED. ) ;
#35912=FACE_OUTER_BOUND ( 'NONE', #47913, .T. ) ;
#35913=CARTESIAN_POINT ( 'NONE',  ( 10.78675619948152864, -17.38023510967517637, 11.49999999999999645 ) ) ;
#35915=AXIS2_PLACEMENT_3D ( 'NONE', #21162, #37898, #98785 ) ;
#35916=DIRECTION ( 'NONE',  ( -3.773278334453079030E-23, 0.9999999999976377785, 2.173523156925979128E-06 ) ) ;
#35917=ORIENTED_EDGE ( 'NONE', *, *, #64959, .F. ) ;
#35919=CARTESIAN_POINT ( 'NONE',  ( -106.6228709571500701, -24.50321055353805022, 9.387540953477515160 ) ) ;
#35920=CARTESIAN_POINT ( 'NONE',  ( -78.62287095715007013, -23.72747288104442021, -1.053458166803662666 ) ) ;
#35921=EDGE_CURVE ( 'NONE', #32470, #11757, #34177, .T. ) ;
#35922=CARTESIAN_POINT ( 'NONE',  ( -41.62287095715006302, -29.50250243563736774, 8.947779886222148704 ) ) ;
#35925=AXIS2_PLACEMENT_3D ( 'NONE', #42778, #11808, #87435 ) ;
#35926=CARTESIAN_POINT ( 'NONE',  ( -10.52143791818333085, 20.43947972196396989, 11.49999999999999645 ) ) ;
#35927=CARTESIAN_POINT ( 'NONE',  ( -16.34568771794417685, -15.85656593008108750, 11.49999999999998934 ) ) ;
#35929=B_SPLINE_CURVE_WITH_KNOTS ( 'NONE', 3,
 ( #80381, #752, #41322, #85990, #71271, #16464 ),
 .UNSPECIFIED., .F., .F.,
 ( 4, 2, 4 ),
 ( 0.000000000000000000, 0.001380901958385391580, 0.002761803916770783161 ),
 .UNSPECIFIED. ) ;
#35930=CARTESIAN_POINT ( 'NONE',  ( -94.52287095715007581, -23.47593901973090524, -1.443836447538996648 ) ) ;
#35931=CARTESIAN_POINT ( 'NONE',  ( -57.52287095715005449, -24.64898659630528854, 1.056161002820822592 ) ) ;
#35933=CARTESIAN_POINT ( 'NONE',  ( -48.62287095715004881, -24.64898659630528144, 1.056161002820821038 ) ) ;
#35934=CARTESIAN_POINT ( 'NONE',  ( -110.5546935055277800, -24.15503026093914229, -0.2815557561904443729 ) ) ;
#35935=CARTESIAN_POINT ( 'NONE',  ( 15.24057855588860377, 15.72025634131890470, 11.49999999999998934 ) ) ;
#35936=EDGE_CURVE ( 'NONE', #56269, #14843, #98308, .T. ) ;
#35938=EDGE_CURVE ( 'NONE', #85031, #59154, #30558, .T. ) ;
#35939=CARTESIAN_POINT ( 'NONE',  ( -28.62287095715004526, -23.57175044478372783, -1.053577738039204847 ) ) ;
#35940=CARTESIAN_POINT ( 'NONE',  ( -71.63959028355270675, -25.28439402384261925, 5.729062157909068809 ) ) ;
#35943=CARTESIAN_POINT ( 'NONE',  ( 16.50020720150075348, -12.08490501797973238, 11.49999999999998934 ) ) ;
#35945=ORIENTED_EDGE ( 'NONE', *, *, #2256, .F. ) ;
#35948=CARTESIAN_POINT ( 'NONE',  ( 21.10734164270438029, -9.282589649079691085, -1.500000000000002220 ) ) ;
#35949=DIRECTION ( 'NONE',  ( -3.773278334453079618E-23, 0.9999999999976377785, 2.173523156925979975E-06 ) ) ;
#35951=CARTESIAN_POINT ( 'NONE',  ( -19.21899500656021331, -6.280627263257740900, -1.500000000000002220 ) ) ;
#35952=ORIENTED_EDGE ( 'NONE', *, *, #78761, .F. ) ;
#35953=DIRECTION ( 'NONE',  ( -3.773278334453079618E-23, 0.9999999999976377785, 2.173523156925979975E-06 ) ) ;
#35954=DIRECTION ( 'NONE',  ( -3.773278334453079030E-23, 0.9999999999976377785, 2.173523156925979128E-06 ) ) ;
#35956=CARTESIAN_POINT ( 'NONE',  ( -95.62858950667747138, -24.63355581998386157, 0.9682620441943944334 ) ) ;
#35957=CARTESIAN_POINT ( 'NONE',  ( -53.54175972517899140, -24.35071581493542681, 9.817618358456032368 ) ) ;
#35958=CARTESIAN_POINT ( 'NONE',  ( 13.34776491790984210, -16.67230741956907991, 11.49999999999999645 ) ) ;
#35960=CARTESIAN_POINT ( 'NONE',  ( -128.6228709571500417, -24.64898659630529565, 1.056161002820834804 ) ) ;
#35961=ORIENTED_EDGE ( 'NONE', *, *, #98794, .T. ) ;
#35962=CARTESIAN_POINT ( 'NONE',  ( 5.670930919660429836, -21.52877996283707418, -1.500000000000002220 ) ) ;
#35963=CARTESIAN_POINT ( 'NONE',  ( -1.398219401198234957, 20.63772364298462847, -1.500000000000002220 ) ) ;
#35965=B_SPLINE_SURFACE_WITH_KNOTS ( 'NONE', 3, 3, ( 
 ( #51190, #59301, #90245, #20720 ),
 ( #75005, #5503, #67420, #28848 ),
 ( #18726, #21710, #29840, #99828 ),
 ( #99342, #84123, #100324, #45580 ),
 ( #15113, #83623, #6509, #22210 ),
 ( #52684, #29339, #44573, #61309 ),
 ( #77499, #14105, #60808, #6002 ) ),
 .UNSPECIFIED., .F., .F., .F.,
 ( 4, 3, 4 ),
 ( 4, 4 ),
 ( 0.7945040050992240310, 0.8970133687736498995, 0.9995227324480757680 ),
 ( 0.3095726639491566123, 0.3107283077887884049 ),
 .UNSPECIFIED. ) ;
#35968=CARTESIAN_POINT ( 'NONE',  ( -129.5228709571500190, -23.94994826722565406, -0.6494450866342675877 ) ) ;
#35969=ORIENTED_EDGE ( 'NONE', *, *, #42597, .T. ) ;
#35970=CARTESIAN_POINT ( 'NONE',  ( 11.42219733811748306, 17.55150860717643724, -1.500000000000002220 ) ) ;
#35971=B_SPLINE_CURVE_WITH_KNOTS ( 'NONE', 3,
 ( #74945, #7943, #48389, #41791, #10821, #15551 ),
 .UNSPECIFIED., .F., .F.,
 ( 4, 2, 4 ),
 ( 1.570755371634033063E-05, 0.001396183895866087103, 0.002776660238015833844 ),
 .UNSPECIFIED. ) ;
#35972=CARTESIAN_POINT ( 'NONE',  ( -1.606994170628035068, 21.82944698466814870, 11.49999999999999645 ) ) ;
#35973=CARTESIAN_POINT ( 'NONE',  ( -37.50484986390183195, -23.96169478059712432, 10.65365249895718591 ) ) ;
#35974=CARTESIAN_POINT ( 'NONE',  ( -15.53634343318938704, 16.32316209468629253, 11.49999999999998934 ) ) ;
#35975=CARTESIAN_POINT ( 'NONE',  ( 20.89173079421859214, 1.537965369061287557, -1.500000000000002220 ) ) ;
#35976=CARTESIAN_POINT ( 'NONE',  ( -80.55620429048342146, -24.99132157543166954, 2.256160258750668834 ) ) ;
#35977=DIRECTION ( 'NONE',  ( 1.000000000000000000, 3.773278334444165844E-23, 8.201307836089272790E-29 ) ) ;
#35978=CARTESIAN_POINT ( 'NONE',  ( -30.64427850938830389, -23.56000036390796737, -1.497999999999532594 ) ) ;
#35979=EDGE_CURVE ( 'NONE', #76617, #87834, #85021, .T. ) ;
#35982=ORIENTED_EDGE ( 'NONE', *, *, #21019, .T. ) ;
#35984=CARTESIAN_POINT ( 'NONE',  ( -128.6228709571500417, -23.96177878511308634, 10.65340807706329151 ) ) ;
#35985=CARTESIAN_POINT ( 'NONE',  ( 14.05358622956002357, 16.19628355576825385, -1.500000000000002220 ) ) ;
#35986=CARTESIAN_POINT ( 'NONE',  ( -127.6228709571500559, -29.50248528299804818, 1.056150453629047137 ) ) ;
#35987=EDGE_LOOP ( 'NONE', ( #3770, #56696, #56709, #52313 ) ) ;
#35988=CARTESIAN_POINT ( 'NONE',  ( -18.71117167593497399, 9.704403692310313190, 11.49999999999998934 ) ) ;
#35989=CARTESIAN_POINT ( 'NONE',  ( -60.52287095715007581, -25.00182538069855198, 7.747789668514453609 ) ) ;
#35990=CARTESIAN_POINT ( 'NONE',  ( -52.62287095715005592, -23.48783264082478794, -1.443836473390070596 ) ) ;
#35991=CARTESIAN_POINT ( 'NONE',  ( -51.62287095715005592, -29.50250243563736774, 8.947779886222146928 ) ) ;
#35993=DIRECTION ( 'NONE',  ( 0.000000000000000000, 0.9999999999976377785, 2.173523156925979128E-06 ) ) ;
#35994=CARTESIAN_POINT ( 'NONE',  ( -21.12782282263547984, 6.412464199276892707, -1.500000000000002220 ) ) ;
#35995=FACE_OUTER_BOUND ( 'NONE', #6623, .T. ) ;
#35996=CARTESIAN_POINT ( 'NONE',  ( -109.0052451887007550, -25.29780460623759808, 4.561057382153821393 ) ) ;
#35997=CARTESIAN_POINT ( 'NONE',  ( -99.52287095715003318, -24.50321055353804667, 9.387540953477522265 ) ) ;
#35998=B_SPLINE_CURVE_WITH_KNOTS ( 'NONE', 3,
 ( #33547, #11210, #64532, #95444, #10714, #41677 ),
 .UNSPECIFIED., .F., .F.,
 ( 4, 2, 4 ),
 ( 1.570755371633718645E-05, 0.001396183895866087103, 0.002776660238015837313 ),
 .UNSPECIFIED. ) ;
#36001=CARTESIAN_POINT ( 'NONE',  ( -14.39514105012195344, 13.04300321504834947, 11.49999999999998934 ) ) ;
#36003=CARTESIAN_POINT ( 'NONE',  ( 21.01207135711032237, 3.775690236426352264, 11.49999999999998934 ) ) ;
#36004=CARTESIAN_POINT ( 'NONE',  ( -123.5228709571500616, -23.47596703998600631, 11.44779298504227860 ) ) ;
#36006=CARTESIAN_POINT ( 'NONE',  ( -64.53959531558551532, -24.51419770103158058, 9.386484678747169852 ) ) ;
#36008=CARTESIAN_POINT ( 'NONE',  ( 22.61563695565308407, -1.323143620866313208, -1.500000000000002220 ) ) ;
#36011=CARTESIAN_POINT ( 'NONE',  ( -87.52287095715009002, -23.96177878511308990, 10.65340807706329862 ) ) ;
#36012=CARTESIAN_POINT ( 'NONE',  ( -79.63744315085436654, -23.96119346886880308, -0.6495511937832122440 ) ) ;
#36013=CARTESIAN_POINT ( 'NONE',  ( -6.535591236171724105, 18.61618873491671877, 11.49999999999999645 ) ) ;
#36016=VERTEX_POINT ( 'NONE', #18997 ) ;
#36017=CARTESIAN_POINT ( 'NONE',  ( -53.62287095715003460, -23.72773821059535493, 11.05748984161097503 ) ) ;
#36018=CARTESIAN_POINT ( 'NONE',  ( -29.22648335530837471, -24.60094061072802063, 2.413927280369137396 ) ) ;
#36019=CARTESIAN_POINT ( 'NONE',  ( -75.52287095715004739, -23.85229601348995487, 10.88205029486208986 ) ) ;
#36020=EDGE_CURVE ( 'NONE', #3816, #59423, #56588, .T. ) ;
#36021=CARTESIAN_POINT ( 'NONE',  ( 0.6597851148675514255, -21.60297929554585394, -1.500000000000002220 ) ) ;
#36022=EDGE_CURVE ( 'NONE', #50770, #57758, #87523, .T. ) ;
#36023=CARTESIAN_POINT ( 'NONE',  ( -26.71664755962209981, -24.80833360015218148, 7.192517110868322128 ) ) ;
#36024=CARTESIAN_POINT ( 'NONE',  ( 12.39309347844599252, 14.90900669795185252, -1.500000000000002220 ) ) ;
#36025=ADVANCED_FACE ( 'NONE', ( #18500 ), #21604, .T. ) ;
#36026=CARTESIAN_POINT ( 'NONE',  ( -50.62287095715005592, -23.47593901973091235, -1.443836447539009749 ) ) ;
#36027=B_SPLINE_CURVE_WITH_KNOTS ( 'NONE', 3,
 ( #13933, #98667, #60139, #12933 ),
 .UNSPECIFIED., .F., .F.,
 ( 4, 4 ),
 ( 6.938893903907228378E-18, 9.999999999999591193E-05 ),
 .UNSPECIFIED. ) ;
#36028=CARTESIAN_POINT ( 'NONE',  ( -66.52287095715006160, -23.48786465467241769, 11.44779295918254647 ) ) ;
#36029=CARTESIAN_POINT ( 'NONE',  ( 19.75791096855702733, 1.210928449428283038, 11.49999999999998934 ) ) ;
#36031=EDGE_CURVE ( 'NONE', #13191, #64103, #57205, .T. ) ;
#36032=CARTESIAN_POINT ( 'NONE',  ( -14.64122064730360862, 14.02963135428074004, 11.49999999999999645 ) ) ;
#36033=CARTESIAN_POINT ( 'NONE',  ( -99.16166289166532977, -25.31166538673566180, 5.311370725864150266 ) ) ;
#36036=ORIENTED_EDGE ( 'NONE', *, *, #17837, .F. ) ;
#36039=CARTESIAN_POINT ( 'NONE',  ( -44.62287095715004881, -23.48783264082478084, -1.443836473390072150 ) ) ;
#36040=B_SPLINE_CURVE_WITH_KNOTS ( 'NONE', 3,
 ( #32549, #63521, #94952, #101, #25438, #94449 ),
 .UNSPECIFIED., .F., .F.,
 ( 4, 2, 4 ),
 ( 1.570887131794333942E-05, 0.001396322306279760422, 0.002776935741241577573 ),
 .UNSPECIFIED. ) ;
#36041=CARTESIAN_POINT ( 'NONE',  ( -92.55620429048339304, -24.66019654487199730, 8.947790411086126383 ) ) ;
#36042=CARTESIAN_POINT ( 'NONE',  ( -85.52287095715006160, -29.50247984919015209, -1.443849546365051806 ) ) ;
#36043=CARTESIAN_POINT ( 'NONE',  ( 18.34943919012036773, 8.063251210807163005, -1.500000000000002220 ) ) ;
#36047=EDGE_CURVE ( 'NONE', #100181, #27742, #23178, .T. ) ;
#36048=CARTESIAN_POINT ( 'NONE',  ( -50.05252738782304789, -25.31297205221429891, 4.679464295789098394 ) ) ;
#36049=VECTOR ( 'NONE', #10441, 1000.000000000000114 ) ;
#36050=DIRECTION ( 'NONE',  ( -3.773278334453079618E-23, 0.9999999999976377785, 2.173523156925979975E-06 ) ) ;
#36053=EDGE_CURVE ( 'NONE', #14276, #52727, #3307, .T. ) ;
#36055=CARTESIAN_POINT ( 'NONE',  ( -19.78178409256797465, 10.57734301857266246, 11.49999999999999645 ) ) ;
#36057=ORIENTED_EDGE ( 'NONE', *, *, #12569, .T. ) ;
#36058=CARTESIAN_POINT ( 'NONE',  ( -2.495337616714382367, -20.20711602426958819, 11.49999999999998934 ) ) ;
#36059=ORIENTED_EDGE ( 'NONE', *, *, #48010, .F. ) ;
#36060=CARTESIAN_POINT ( 'NONE',  ( 22.95104020007722667, -0.4190376320207603866, -1.500000000000002220 ) ) ;
#36061=EDGE_CURVE ( 'NONE', #30291, #30754, #89881, .T. ) ;
#36064=CARTESIAN_POINT ( 'NONE',  ( -109.5228709571501327, -23.96127896941632685, -0.6493128931037961404 ) ) ;
#36065=ADVANCED_FACE ( 'NONE', ( #43353 ), #73787, .F. ) ;
#36066=CARTESIAN_POINT ( 'NONE',  ( -77.55422458372758854, -23.96169478059713498, 10.65365249895717703 ) ) ;
#36068=ADVANCED_FACE ( 'NONE', ( #81408 ), #83173, .T. ) ;
#36069=CARTESIAN_POINT ( 'NONE',  ( -117.5895376238167245, -23.48786465467241769, 11.44779295918253759 ) ) ;
#36070=CARTESIAN_POINT ( 'NONE',  ( -21.08860491664495029, 2.407354197416772035, 11.49999999999999645 ) ) ;
#36073=ORIENTED_EDGE ( 'NONE', *, *, #52474, .T. ) ;
#36074=CARTESIAN_POINT ( 'NONE',  ( 4.260453091581613450, -21.75001586557718980, 11.49999999999998934 ) ) ;
#36075=B_SPLINE_CURVE_WITH_KNOTS ( 'NONE', 3,
 ( #24384, #38105, #22860, #39609 ),
 .UNSPECIFIED., .F., .F.,
 ( 4, 4 ),
 ( 0.07984293836553946200, 0.08884936963765502349 ),
 .UNSPECIFIED. ) ;
#36076=CARTESIAN_POINT ( 'NONE',  ( -6.273408026305254737, 19.60348359158234288, -1.500000000000002220 ) ) ;
#36078=VECTOR ( 'NONE', #44645, 1000.000000000000114 ) ;
#36081=CARTESIAN_POINT ( 'NONE',  ( -126.6228709571500843, -24.51387760970726859, 9.387446482453416507 ) ) ;
#36082=EDGE_LOOP ( 'NONE', ( #57900, #61335, #71592, #58692 ) ) ;
#36083=EDGE_LOOP ( 'NONE', ( #52263, #37668, #73649, #14013 ) ) ;
#36084=ORIENTED_EDGE ( 'NONE', *, *, #53589, .T. ) ;
#36085=VECTOR ( 'NONE', #39854, 1000.000000000000114 ) ;
#36087=CARTESIAN_POINT ( 'NONE',  ( -28.66135699505452550, -23.58527356016855236, 11.05961558438220749 ) ) ;
#36088=CARTESIAN_POINT ( 'NONE',  ( -130.5728709571500588, -23.56000036390796737, 11.50200000000000244 ) ) ;
#36089=CARTESIAN_POINT ( 'NONE',  ( 1.902724757927627408, 20.64897553884969028, -1.500000000000002220 ) ) ;
#36090=CARTESIAN_POINT ( 'NONE',  ( -13.51661872714272405, -17.00040112538478709, 11.49999999999999645 ) ) ;
#36091=ORIENTED_EDGE ( 'NONE', *, *, #40556, .T. ) ;
#36092=CARTESIAN_POINT ( 'NONE',  ( -40.91098280806539833, -25.27806118004114211, 4.981854051466827471 ) ) ;
#36093=CARTESIAN_POINT ( 'NONE',  ( -77.55620429048339304, -23.48786465467241058, 11.44779295918254469 ) ) ;
#36094=CARTESIAN_POINT ( 'NONE',  ( -115.5902995085408094, -24.40034930558991277, 0.3402023900116066257 ) ) ;
#36095=CARTESIAN_POINT ( 'NONE',  ( -0.1411031551986380028, 22.44022050402121948, -1.500000000000002220 ) ) ;
#36097=CARTESIAN_POINT ( 'NONE',  ( -124.5228709571500900, -24.35013146730205236, 9.818937971375092388 ) ) ;
#36099=CARTESIAN_POINT ( 'NONE',  ( -71.33442243081988465, -25.31573830894388166, 5.086045725258812489 ) ) ;
#36103=CARTESIAN_POINT ( 'NONE',  ( -46.51385822909820433, -23.73791477778911840, 11.05961554403171299 ) ) ;
#36104=ORIENTED_EDGE ( 'NONE', *, *, #8293, .F. ) ;
#36106=CARTESIAN_POINT ( 'NONE',  ( 14.87313431965483801, 15.23822737908125902, -1.500000000000002220 ) ) ;
#36107=VERTEX_POINT ( 'NONE', #76267 ) ;
#36108=CARTESIAN_POINT ( 'NONE',  ( -41.52287095715006870, -24.64965694238406613, 8.947790433994205372 ) ) ;
#36110=CARTESIAN_POINT ( 'NONE',  ( -5.042499505632127565, 21.24692939306837758, -1.500000000000002220 ) ) ;
#36111=CARTESIAN_POINT ( 'NONE',  ( -101.6228709571500559, -29.50250243563736774, 8.947779886222138046 ) ) ;
#36112=CARTESIAN_POINT ( 'NONE',  ( 22.70222466501550329, 0.2752559529566028229, -1.500000000000002220 ) ) ;
#36113=CARTESIAN_POINT ( 'NONE',  ( -40.49257998994310270, -25.28892422309372634, 3.294941674263239140 ) ) ;
#36115=CARTESIAN_POINT ( 'NONE',  ( 20.57779966680088890, -7.652443150423321683, -1.500000000000002220 ) ) ;
#36116=CARTESIAN_POINT ( 'NONE',  ( -87.62875567979766345, -24.34968618360935011, 0.1864209137778971292 ) ) ;
#36117=EDGE_LOOP ( 'NONE', ( #55579, #39171, #19839, #18973 ) ) ;
#36118=CARTESIAN_POINT ( 'NONE',  ( -40.17570312657086617, -25.29422630904218039, 5.527950596489476176 ) ) ;
#36123=CARTESIAN_POINT ( 'NONE',  ( -84.55445823045992881, -23.96169478059713498, 10.65365249895717881 ) ) ;
#36124=B_SPLINE_CURVE_WITH_KNOTS ( 'NONE', 3,
 ( #44950, #84490, #78859, #33201 ),
 .UNSPECIFIED., .F., .F.,
 ( 4, 4 ),
 ( 0.3707647540354188642, 0.3797711853075343980 ),
 .UNSPECIFIED. ) ;
#36126=DIRECTION ( 'NONE',  ( -3.773278334453079618E-23, 0.9999999999976377785, 2.173523156925978705E-06 ) ) ;
#36127=CARTESIAN_POINT ( 'NONE',  ( -20.45437310074456860, -23.26047912157225994, -0.4716817114508955466 ) ) ;
#36128=CARTESIAN_POINT ( 'NONE',  ( -16.85803360905838488, 12.98640638483674259, -1.500000000000002220 ) ) ;
#36129=CARTESIAN_POINT ( 'NONE',  ( -98.58670432545206097, -24.51419770103156992, 9.386484678747175181 ) ) ;
#36131=CARTESIAN_POINT ( 'NONE',  ( -70.32380231474228083, -29.50249842297920466, 7.101626040072651413 ) ) ;
#36132=CARTESIAN_POINT ( 'NONE',  ( -85.62287095715007013, -23.84081130438200802, 10.88220057463249546 ) ) ;
#36133=CARTESIAN_POINT ( 'NONE',  ( -90.58953762381672448, -24.99132157543084531, 2.256160258750496972 ) ) ;
#36134=EDGE_LOOP ( 'NONE', ( #26857, #12355, #58587, #60188 ) ) ;
#36135=ADVANCED_FACE ( 'NONE', ( #70167 ), #14869, .F. ) ;
#36136=CARTESIAN_POINT ( 'NONE',  ( -1.979602623192304955, -19.45764201480039901, 11.49999999999999645 ) ) ;
#36137=CARTESIAN_POINT ( 'NONE',  ( -99.12672508963875373, -25.28202003831819056, 4.094530911986962174 ) ) ;
#36140=ORIENTED_EDGE ( 'NONE', *, *, #49972, .F. ) ;
#36141=ADVANCED_FACE ( 'NONE', ( #62566 ), #61572, .F. ) ;
#36143=CARTESIAN_POINT ( 'NONE',  ( -99.33274021282838362, -25.25095929706067821, 5.901068790733613234 ) ) ;
#36144=EDGE_CURVE ( 'NONE', #803, #77182, #42637, .T. ) ;
#36145=CARTESIAN_POINT ( 'NONE',  ( -25.67705512370713095, -24.85598980928401147, 6.414578969243027728 ) ) ;
#36146=EDGE_CURVE ( 'NONE', #32109, #79759, #99550, .T. ) ;
#36148=CARTESIAN_POINT ( 'NONE',  ( -45.62287095715006302, -24.82558206586143612, 1.605769216559445045 ) ) ;
#36149=CARTESIAN_POINT ( 'NONE',  ( -10.80270875523330965, -16.48872379891551532, -1.500000000000002220 ) ) ;
#36152=CARTESIAN_POINT ( 'NONE',  ( -108.5228709571500616, -23.47596703998600631, 11.44779298504228038 ) ) ;
#36157=CARTESIAN_POINT ( 'NONE',  ( -54.52287095715006870, -24.64965694238575011, 8.947790433994203596 ) ) ;
#36159=CARTESIAN_POINT ( 'NONE',  ( -47.57719180744601317, -24.65952944569304606, 1.056160979905696129 ) ) ;
#36162=DIRECTION ( 'NONE',  ( 0.000000000000000000, -0.9999999999976377785, -2.173523156925979975E-06 ) ) ;
#36163=AXIS2_PLACEMENT_3D ( 'NONE', #15616, #80025, #41469 ) ;
#36164=CARTESIAN_POINT ( 'NONE',  ( -91.52287095715006160, -24.64965694238575011, 8.947790433994196491 ) ) ;
#36165=CARTESIAN_POINT ( 'NONE',  ( -15.85412420263326538, -12.13584807887712458, -1.500000000000002220 ) ) ;
#36166=ADVANCED_FACE ( 'NONE', ( #78259 ), #95169, .T. ) ;
#36168=CARTESIAN_POINT ( 'NONE',  ( -0.02330722796118872564, -22.74826961827042382, 7.709244911848460724 ) ) ;
#36169=ORIENTED_EDGE ( 'NONE', *, *, #17709, .T. ) ;
#36173=CARTESIAN_POINT ( 'NONE',  ( -107.2228709571500929, -23.47593901973090169, -1.443836447538996648 ) ) ;
#36174=CARTESIAN_POINT ( 'NONE',  ( -80.55868461798210944, -23.85049219812685806, 10.88485053497527311 ) ) ;
#36176=CARTESIAN_POINT ( 'NONE',  ( -39.64841240158730074, -23.96119346886879597, -0.6495511937832143534 ) ) ;
#36177=CARTESIAN_POINT ( 'NONE',  ( -26.09950011358278843, -24.96552080349164981, 4.651270459924270462 ) ) ;
#36179=ORIENTED_EDGE ( 'NONE', *, *, #14227, .F. ) ;
#36180=B_SPLINE_SURFACE_WITH_KNOTS ( 'NONE', 3, 3, ( 
 ( #68591, #85815, #99515, #60985 ),
 ( #84299, #14786, #45752, #100007 ),
 ( #56389, #72603, #87821, #18308 ),
 ( #64009, #41154, #63503, #48264 ),
 ( #9184, #24906, #18797, #86312 ),
 ( #33530, #41656, #25915, #78678 ),
 ( #17299, #40145, #87311, #2593 ) ),
 .UNSPECIFIED., .F., .F., .F.,
 ( 4, 3, 4 ),
 ( 4, 4 ),
 ( 0.7945040050992233649, 0.8970133687736493444, 0.9995227324480753239 ),
 ( 0.05950911933808800819, 0.06054931725151718042 ),
 .UNSPECIFIED. ) ;
#36181=CARTESIAN_POINT ( 'NONE',  ( -37.62287095715005592, -24.64965695001467694, 8.947790433994187609 ) ) ;
#36183=ORIENTED_EDGE ( 'NONE', *, *, #33054, .F. ) ;
#36184=CARTESIAN_POINT ( 'NONE',  ( -6.993686169601437186, 18.98418669460116348, -1.500000000000002220 ) ) ;
#36185=CARTESIAN_POINT ( 'NONE',  ( -43.52287095715004739, -23.48783264083374078, -1.443836473376152840 ) ) ;
#36188=CARTESIAN_POINT ( 'NONE',  ( -82.58953762381673869, -24.66019654487199730, 8.947790411086119278 ) ) ;
#36189=ADVANCED_FACE ( 'NONE', ( #23467 ), #85382, .T. ) ;
#36190=ORIENTED_EDGE ( 'NONE', *, *, #97028, .T. ) ;
#36193=CARTESIAN_POINT ( 'NONE',  ( 11.39338536883839659, -16.50304575528446804, -1.500000000000002220 ) ) ;
#36195=CARTESIAN_POINT ( 'NONE',  ( 21.00884048613226440, 1.293913838035418040, 11.49999999999999645 ) ) ;
#36197=CARTESIAN_POINT ( 'NONE',  ( -70.58187708969072105, -24.83644354573578994, 8.397322867130100121 ) ) ;
#36198=CARTESIAN_POINT ( 'NONE',  ( -7.692412698405892257, 20.70400481474656118, -1.500000000000002220 ) ) ;
#36199=EDGE_CURVE ( 'NONE', #39807, #19418, #20855, .T. ) ;
#36201=CARTESIAN_POINT ( 'NONE',  ( -76.52287095715007581, -23.47593901973090169, -1.443836447538996648 ) ) ;
#36202=CARTESIAN_POINT ( 'NONE',  ( -64.55620429048339304, -23.47596703998600276, 11.44779298504227505 ) ) ;
#36203=ORIENTED_EDGE ( 'NONE', *, *, #69702, .F. ) ;
#36205=CARTESIAN_POINT ( 'NONE',  ( -31.53142997842084938, -24.51314013834316086, 0.6176544820404139546 ) ) ;
#36210=CARTESIAN_POINT ( 'NONE',  ( -89.62287095715004170, -24.65952944569305316, 1.056160979905700348 ) ) ;
#36211=CARTESIAN_POINT ( 'NONE',  ( -19.86366060283327784, 5.362777492974458049, -1.500000000000002220 ) ) ;
#36212=CARTESIAN_POINT ( 'NONE',  ( -16.60028029328060128, 13.79055755010687356, 11.49999999999999645 ) ) ;
#36213=EDGE_LOOP ( 'NONE', ( #87432, #1447, #14166, #60822 ) ) ;
#36214=CARTESIAN_POINT ( 'NONE',  ( -91.63754064921776887, -23.73766607897670156, -1.055555164236454235 ) ) ;
#36215=CARTESIAN_POINT ( 'NONE',  ( -128.5228709571500758, -29.50247984919015209, -1.443849546365044922 ) ) ;
#36216=CARTESIAN_POINT ( 'NONE',  ( -129.6228709571500133, -24.51283580621365132, 0.6167428607019831421 ) ) ;
#36217=CARTESIAN_POINT ( 'NONE',  ( -15.79502933763849271, 15.79022959414610661, 11.49999999999998934 ) ) ;
#36219=CARTESIAN_POINT ( 'NONE',  ( -114.6228709571500559, -29.50248528299804818, 1.056150453629043584 ) ) ;
#36220=CARTESIAN_POINT ( 'NONE',  ( -84.51766577851211082, -23.73766607897669445, -1.055555164236457344 ) ) ;
#36221=ORIENTED_EDGE ( 'NONE', *, *, #12024, .T. ) ;
#36224=CARTESIAN_POINT ( 'NONE',  ( 18.69404101259207707, 9.334567778723176446, -1.500000000000002220 ) ) ;
#36225=ORIENTED_EDGE ( 'NONE', *, *, #71603, .T. ) ;
#36226=CARTESIAN_POINT ( 'NONE',  ( -39.32675481643261861, -25.19484965671346188, 3.363571302307362565 ) ) ;
#36227=EDGE_LOOP ( 'NONE', ( #85357, #42123, #70185, #18582 ) ) ;
#36230=CARTESIAN_POINT ( 'NONE',  ( -100.5053545878111407, -24.92592662359561473, 8.075495903018000021 ) ) ;
#36231=CARTESIAN_POINT ( 'NONE',  ( 9.152908845159860363, 19.05633030926415472, -1.500000000000002220 ) ) ;
#36232=B_SPLINE_CURVE_WITH_KNOTS ( 'NONE', 3,
 ( #25810, #89212, #72997, #3486, #96816, #34424 ),
 .UNSPECIFIED., .F., .F.,
 ( 4, 2, 4 ),
 ( 0.000000000000000000, 0.001380764517854765182, 0.002761529035709530365 ),
 .UNSPECIFIED. ) ;
#36234=CARTESIAN_POINT ( 'NONE',  ( -123.5228709571500616, -23.47596703998600631, 11.44779298504227860 ) ) ;
#36236=CARTESIAN_POINT ( 'NONE',  ( -110.6167804036481925, -25.20868619939636091, 6.586938478111401984 ) ) ;
#36237=B_SPLINE_CURVE_WITH_KNOTS ( 'NONE', 3,
 ( #65676, #3269, #50429, #81371 ),
 .UNSPECIFIED., .F., .F.,
 ( 4, 4 ),
 ( 0.1599001052287878089, 0.1689065365009033703 ),
 .UNSPECIFIED. ) ;
#36239=CARTESIAN_POINT ( 'NONE',  ( -76.54601064557617462, -24.35071581493543036, 9.817618358456028815 ) ) ;
#36240=B_SPLINE_CURVE_WITH_KNOTS ( 'NONE', 3,
 ( #17374, #71169, #644, #39703, #9254, #48337 ),
 .UNSPECIFIED., .F., .F.,
 ( 4, 2, 4 ),
 ( 0.000000000000000000, 0.001380901958385385509, 0.002761803916770771018 ),
 .UNSPECIFIED. ) ;
#36242=CARTESIAN_POINT ( 'NONE',  ( -21.33044368757495590, -4.375833669458513597, -1.500000000000002220 ) ) ;
#36243=CARTESIAN_POINT ( 'NONE',  ( -78.94303308397304875, -25.27645460285955181, 5.977536667781793156 ) ) ;
#36244=CARTESIAN_POINT ( 'NONE',  ( -15.79502933763849271, 15.79022959414610661, 11.49999999999999645 ) ) ;
#36246=CARTESIAN_POINT ( 'NONE',  ( -116.6228709571500559, -23.47593901973091235, -1.443836447538997536 ) ) ;
#36248=CARTESIAN_POINT ( 'NONE',  ( -31.55620429048340014, -24.64898659630528144, 1.056161002820817263 ) ) ;
#36249=EDGE_LOOP ( 'NONE', ( #86496, #46934, #65019, #43044 ) ) ;
#36250=VERTEX_POINT ( 'NONE', #48849 ) ;
#36252=CARTESIAN_POINT ( 'NONE',  ( -116.5228709571500616, -23.47596703998600631, 11.44779298504227860 ) ) ;
#36256=CARTESIAN_POINT ( 'NONE',  ( -1.480291460309441920, -19.30061035156251847, 11.49999999999998934 ) ) ;
#36258=ORIENTED_EDGE ( 'NONE', *, *, #85502, .T. ) ;
#36259=ADVANCED_FACE ( 'NONE', ( #70669 ), #18383, .T. ) ;
#36260=CARTESIAN_POINT ( 'NONE',  ( -19.35591191756920892, -0.7100623379298715010, 11.49999999999999645 ) ) ;
#36261=PLANE ( 'NONE',  #13104 ) ;
#36262=ORIENTED_EDGE ( 'NONE', *, *, #67007, .F. ) ;
#36268=EDGE_CURVE ( 'NONE', #21016, #12190, #76567, .T. ) ;
#36269=PLANE ( 'NONE',  #52077 ) ;
#36270=CARTESIAN_POINT ( 'NONE',  ( 18.24213732562919787, -7.162457363581539838, 11.49999999999998934 ) ) ;
#36275=CARTESIAN_POINT ( 'NONE',  ( -20.03152041342270806, -8.007337437543776915, -1.500000000000002220 ) ) ;
#36276=CARTESIAN_POINT ( 'NONE',  ( -33.57065171927310132, -23.48786465467240347, 11.44779295918255535 ) ) ;
#36277=ADVANCED_FACE ( 'NONE', ( #79273 ), #86888, .T. ) ;
#36278=CARTESIAN_POINT ( 'NONE',  ( -40.52287095715005449, -24.99132157543166244, 2.256160258750667502 ) ) ;
#36279=PLANE ( 'NONE',  #65454 ) ;
#36281=B_SPLINE_CURVE_WITH_KNOTS ( 'NONE', 3,
 ( #8306, #39248, #31635, #47376, #8810, #3706 ),
 .UNSPECIFIED., .F., .F.,
 ( 4, 2, 4 ),
 ( 0.000000000000000000, 0.001380764517854768652, 0.002761529035709537304 ),
 .UNSPECIFIED. ) ;
#36282=CARTESIAN_POINT ( 'NONE',  ( 21.12055942831636202, -9.126644407798330860, -1.500000000000002220 ) ) ;
#36286=CARTESIAN_POINT ( 'NONE',  ( -18.22032804147677254, 8.545885342870345625, 11.49999999999999645 ) ) ;
#36287=CARTESIAN_POINT ( 'NONE',  ( -101.5895376238167245, -24.64898659630368627, 1.056161002820391381 ) ) ;
#36288=CARTESIAN_POINT ( 'NONE',  ( -32.61006605916473688, -23.73791477778911485, 11.05961554403171299 ) ) ;
#36292=CARTESIAN_POINT ( 'NONE',  ( 1.822157996128044299, -19.77364354024053839, -1.500000000000002220 ) ) ;
#36293=VECTOR ( 'NONE', #88121, 1000.000000000000114 ) ;
#36294=CARTESIAN_POINT ( 'NONE',  ( -47.55620429048339304, -24.66019654487199020, 8.947790411086135265 ) ) ;
#36295=CARTESIAN_POINT ( 'NONE',  ( -12.15653940608521566, -15.58205587995076868, -1.500000000000002220 ) ) ;
#36296=ADVANCED_FACE ( 'NONE', ( #16874 ), #17886, .F. ) ;
#36300=CARTESIAN_POINT ( 'NONE',  ( -12.00526669028610272, -16.82065764665920682, 11.49999999999999645 ) ) ;
#36304=CARTESIAN_POINT ( 'NONE',  ( -11.22117850230010738, 19.66027149220947123, 11.49999999999999645 ) ) ;
#36305=EDGE_LOOP ( 'NONE', ( #73452, #59095, #36420, #94102 ) ) ;
#36306=CARTESIAN_POINT ( 'NONE',  ( -107.5228709571500758, -29.50250786944525672, 11.44777988621622988 ) ) ;
#36308=DIRECTION ( 'NONE',  ( -1.000000000000000000, -3.773278334444167608E-23, -8.201307833595939069E-29 ) ) ;
#36310=B_SPLINE_CURVE_WITH_KNOTS ( 'NONE', 3,
 ( #47793, #9212, #94959, #70622, #93952, #18338 ),
 .UNSPECIFIED., .F., .F.,
 ( 4, 2, 4 ),
 ( 1.570755371633698994E-05, 0.001396183895866086235, 0.002776660238015835579 ),
 .UNSPECIFIED. ) ;
#36312=EDGE_LOOP ( 'NONE', ( #42585, #8156, #35359, #78476 ) ) ;
#36313=CARTESIAN_POINT ( 'NONE',  ( -99.90107996939670443, -25.13963275720788815, 7.004612396290182730 ) ) ;
#36314=CARTESIAN_POINT ( 'NONE',  ( -20.40978113611479827, 10.34812579263477872, -1.500000000000002220 ) ) ;
#36315=FACE_OUTER_BOUND ( 'NONE', #37381, .T. ) ;
#36316=CARTESIAN_POINT ( 'NONE',  ( 21.55061338234859392, -0.003183148592148328428, -1.500000000000002220 ) ) ;
#36318=CARTESIAN_POINT ( 'NONE',  ( -65.52287095715011844, -24.83602698348160231, 1.605859176311265735 ) ) ;
#36320=CARTESIAN_POINT ( 'NONE',  ( -11.40494320173684351, 19.43794304404440254, 11.49999999999999645 ) ) ;
#36321=EDGE_LOOP ( 'NONE', ( #76900, #32969, #39836, #28612 ) ) ;
#36322=CARTESIAN_POINT ( 'NONE',  ( -32.62287095715004881, -29.50250243563736774, 8.947779886222150481 ) ) ;
#36323=CARTESIAN_POINT ( 'NONE',  ( 21.66556372666567754, 3.824538051775513647, 11.49999999999998934 ) ) ;
#36324=CARTESIAN_POINT ( 'NONE',  ( -105.5487305842052308, -24.73531770709095312, 8.716586749053508498 ) ) ;
#36325=CARTESIAN_POINT ( 'NONE',  ( -28.81656857143860861, -24.79700183405136116, 6.988807522033142483 ) ) ;
#36327=CARTESIAN_POINT ( 'NONE',  ( -48.61472421919472708, -23.48786465467241058, 11.44779295918254824 ) ) ;
#36328=EDGE_CURVE ( 'NONE', #43445, #29369, #32605, .T. ) ;
#36329=CARTESIAN_POINT ( 'NONE',  ( -90.54956613838091073, -24.40133493613049964, 9.663955038902805939 ) ) ;
#36331=FACE_OUTER_BOUND ( 'NONE', #82619, .T. ) ;
#36334=CARTESIAN_POINT ( 'NONE',  ( -126.5228709571500048, -23.94994826722564696, -0.6494450866342701412 ) ) ;
#36335=PLANE ( 'NONE',  #14619 ) ;
#36336=CARTESIAN_POINT ( 'NONE',  ( -36.66654255312141686, -23.48783264082477018, -1.443836473390095909 ) ) ;
#36337=CARTESIAN_POINT ( 'NONE',  ( 12.54693703879240196, 16.07252283493236433, -1.500000000000002220 ) ) ;
#36338=ADVANCED_FACE ( 'NONE', ( #56465 ), #72183, .T. ) ;
#36342=CARTESIAN_POINT ( 'NONE',  ( -30.59755354180557418, -24.77158516743337913, 8.907023374642850655 ) ) ;
#36343=CARTESIAN_POINT ( 'NONE',  ( -108.6228709571500559, -29.50248528299804818, 1.056150453629043584 ) ) ;
#36347=CARTESIAN_POINT ( 'NONE',  ( -28.13918514477506250, -24.63646054457999668, 8.204675463703699378 ) ) ;
#36348=CARTESIAN_POINT ( 'NONE',  ( -8.262104503270727207, -19.10415460921518971, 11.49999999999998934 ) ) ;
#36353=B_SPLINE_CURVE_WITH_KNOTS ( 'NONE', 3,
 ( #28879, #44607, #75534, #65475, #37490, #100358 ),
 .UNSPECIFIED., .F., .F.,
 ( 4, 2, 4 ),
 ( 0.000000000000000000, 0.001380901958385381606, 0.002761803916770763211 ),
 .UNSPECIFIED. ) ;
#36355=FACE_OUTER_BOUND ( 'NONE', #82144, .T. ) ;
#36357=VERTEX_POINT ( 'NONE', #1163 ) ;
#36358=CARTESIAN_POINT ( 'NONE',  ( -78.62287095715007013, -23.73907113216991860, -1.053371485793229700 ) ) ;
#36359=CARTESIAN_POINT ( 'NONE',  ( -64.52287095715007581, -24.35013146730204170, 9.818937971375095941 ) ) ;
#36361=CARTESIAN_POINT ( 'NONE',  ( -74.62287095715005592, -23.47593901973091235, -1.443836447539006196 ) ) ;
#36362=CARTESIAN_POINT ( 'NONE',  ( -10.56713949322891999, -19.48831581008217384, 11.49999999999999645 ) ) ;
#36363=VERTEX_POINT ( 'NONE', #24984 ) ;
#36364=B_SPLINE_CURVE_WITH_KNOTS ( 'NONE', 3,
 ( #7921, #23632, #76420, #15028 ),
 .UNSPECIFIED., .F., .F.,
 ( 4, 4 ),
 ( 0.5491634581351279021, 0.5501642051758932617 ),
 .UNSPECIFIED. ) ;
#36365=CARTESIAN_POINT ( 'NONE',  ( -108.6247772082418948, -24.51314013834316086, 0.6176544820404235026 ) ) ;
#36366=CARTESIAN_POINT ( 'NONE',  ( 11.26306171725914851, -19.60737681494043727, 11.49999999999998934 ) ) ;
#36367=CARTESIAN_POINT ( 'NONE',  ( -115.5917237373192989, -24.15602025860897584, 10.28564288303533836 ) ) ;
#36368=ORIENTED_EDGE ( 'NONE', *, *, #6475, .F. ) ;
#36370=CARTESIAN_POINT ( 'NONE',  ( -71.52287095715007581, -29.50250243563736774, 8.947779886222143375 ) ) ;
#36372=CARTESIAN_POINT ( 'NONE',  ( -28.52287095715005094, -23.31182002239687989, -1.443836447538998202 ) ) ;
#36375=CARTESIAN_POINT ( 'NONE',  ( 7.309977242446557888, -21.02818303981469583, -1.500000000000002220 ) ) ;
#36376=CARTESIAN_POINT ( 'NONE',  ( -50.40895856474225667, -25.13941497071981246, 7.563173984875121825 ) ) ;
#36379=CARTESIAN_POINT ( 'NONE',  ( -120.6228709571500417, -29.50247984919015209, -1.443849546365046699 ) ) ;
#36380=CARTESIAN_POINT ( 'NONE',  ( -26.97479289097202582, -24.58642771986267661, 1.762362389447201805 ) ) ;
#36381=DIRECTION ( 'NONE',  ( 1.000000000000000000, 3.773278334444167608E-23, 8.201307810031802745E-29 ) ) ;
#36382=CARTESIAN_POINT ( 'NONE',  ( -73.55620429048340725, -24.64965694238574656, 8.947790433994198267 ) ) ;
#36383=CARTESIAN_POINT ( 'NONE',  ( -17.32436372870746055, -8.985247798433253053, 11.49999999999998934 ) ) ;
#36385=CARTESIAN_POINT ( 'NONE',  ( -19.15072323977689095, -9.709862252083167888, 11.49999999999998934 ) ) ;
#36386=CARTESIAN_POINT ( 'NONE',  ( -25.56915516548917822, -24.58000038722270020, 4.121107147866038822 ) ) ;
#36389=CARTESIAN_POINT ( 'NONE',  ( -85.52287095715006160, -23.48786465467241058, 11.44779295918254292 ) ) ;
#36390=CARTESIAN_POINT ( 'NONE',  ( -10.92962168092244823, 19.99562239114850826, -1.500000000000002220 ) ) ;
#36391=VECTOR ( 'NONE', #19682, 1000.000000000000114 ) ;
#36395=CARTESIAN_POINT ( 'NONE',  ( -18.23705311251027794, 8.147635122911419003, 11.49999999999999645 ) ) ;
#36396=CARTESIAN_POINT ( 'NONE',  ( -50.52287095715005449, -24.83602698348160231, 1.605859176311259073 ) ) ;
#36397=CARTESIAN_POINT ( 'NONE',  ( -74.58443573574729157, -24.51419770103159124, 9.386484678747162747 ) ) ;
#36400=ADVANCED_FACE ( 'NONE', ( #38834 ), #6889, .F. ) ;
#36401=CARTESIAN_POINT ( 'NONE',  ( -27.61157986406360365, -24.60851323062442475, 1.630394788138983753 ) ) ;
#36403=AXIS2_PLACEMENT_3D ( 'NONE', #65550, #89358, #49820 ) ;
#36404=CARTESIAN_POINT ( 'NONE',  ( 21.66353188042378974, 1.267531592894010739, -1.500000000000002220 ) ) ;
#36405=CARTESIAN_POINT ( 'NONE',  ( -60.58953762381672448, -25.00158670708909270, 2.256160236439167299 ) ) ;
#36406=CARTESIAN_POINT ( 'NONE',  ( -16.16875682573952133, 10.94412424577950915, -1.500000000000002220 ) ) ;
#36407=CARTESIAN_POINT ( 'NONE',  ( -99.30650101624107151, -25.24758513798436610, 6.287525626990708716 ) ) ;
#36410=CARTESIAN_POINT ( 'NONE',  ( -108.8968792378191921, -25.05712065398430966, 7.447789548358837663 ) ) ;
#36412=CARTESIAN_POINT ( 'NONE',  ( 12.80116962295325322, 15.99954467330607244, 11.49999999999999645 ) ) ;
#36413=CARTESIAN_POINT ( 'NONE',  ( -49.73739581626914230, -25.30026926557708578, 5.371920104873852075 ) ) ;
#36414=CARTESIAN_POINT ( 'NONE',  ( -40.55620429048340725, -23.48783264082477729, -1.443836473390073705 ) ) ;
#36417=CARTESIAN_POINT ( 'NONE',  ( -106.6228709571500559, -23.47596703998600631, 11.44779298504227860 ) ) ;
#36418=CARTESIAN_POINT ( 'NONE',  ( -114.5228709571500758, -23.47593901973090524, -1.443836447538996204 ) ) ;
#36420=ORIENTED_EDGE ( 'NONE', *, *, #38473, .T. ) ;
#36422=EDGE_CURVE ( 'NONE', #58657, #82541, #70481, .T. ) ;
#36423=CARTESIAN_POINT ( 'NONE',  ( -13.44081803467414638, 18.71018530922267686, 11.49999999999999645 ) ) ;
#36424=CARTESIAN_POINT ( 'NONE',  ( -13.85039312988123150, 18.09399583546626289, 11.49999999999998934 ) ) ;
#36426=CARTESIAN_POINT ( 'NONE',  ( -40.52287095715006870, -23.47593901973090169, -1.443836447538997092 ) ) ;
#36427=DIRECTION ( 'NONE',  ( 1.000000000000000000, 3.773278334444166432E-23, 8.201307841325785021E-29 ) ) ;
#36430=CARTESIAN_POINT ( 'NONE',  ( -110.5141208177188048, -24.52300882791530512, 0.6510814631126329299 ) ) ;
#36431=CARTESIAN_POINT ( 'NONE',  ( 4.863445656156933694, -21.36585520573490626, -1.500000000000002220 ) ) ;
#36432=EDGE_CURVE ( 'NONE', #27620, #21016, #37356, .T. ) ;
#36435=CARTESIAN_POINT ( 'NONE',  ( -58.62287095715004881, -29.50250243563736774, 8.947779886222145151 ) ) ;
#36436=CARTESIAN_POINT ( 'NONE',  ( -94.62287095715005592, -24.66019654487199730, 8.947790411086126383 ) ) ;
#36438=VERTEX_POINT ( 'NONE', #91619 ) ;
#36439=CARTESIAN_POINT ( 'NONE',  ( -1.999887071766271784, 20.33596237858139233, -1.500000000000002220 ) ) ;
#36440=ORIENTED_EDGE ( 'NONE', *, *, #46920, .T. ) ;
#36441=B_SPLINE_CURVE_WITH_KNOTS ( 'NONE', 3,
 ( #91208, #8478, #83590, #76472, #21683, #7971, #52654, #14581 ),
 .UNSPECIFIED., .F., .F.,
 ( 4, 2, 2, 4 ),
 ( 0.000000000000000000, 0.002001098010032797709, 0.003001647015049196780, 0.004002196020065595418 ),
 .UNSPECIFIED. ) ;
#36442=ORIENTED_EDGE ( 'NONE', *, *, #87942, .T. ) ;
#36445=CARTESIAN_POINT ( 'NONE',  ( -17.35246277222573141, 15.15038115719275424, 11.49999999999998934 ) ) ;
#36446=CARTESIAN_POINT ( 'NONE',  ( -61.49452177658557872, -24.51314013834316086, 0.6176544820404138436 ) ) ;
#36447=CARTESIAN_POINT ( 'NONE',  ( -0.6865706486018943178, -20.24796467851281179, -1.500000000000002220 ) ) ;
#36448=VERTEX_POINT ( 'NONE', #23595 ) ;
#36449=CARTESIAN_POINT ( 'NONE',  ( -27.13986186919794008, -25.04474643995085614, 5.848370260082334404 ) ) ;
#36450=CARTESIAN_POINT ( 'NONE',  ( -87.62287095715001328, -23.48786465467241769, 11.44779295918254114 ) ) ;
#36451=CARTESIAN_POINT ( 'NONE',  ( -95.62584188182231060, -24.83618233451450408, 1.606449574219538157 ) ) ;
#36452=CARTESIAN_POINT ( 'NONE',  ( -41.62287095715006302, -24.33927499327853639, 9.819080762295824272 ) ) ;
#36453=CARTESIAN_POINT ( 'NONE',  ( 5.910897418159350103, -20.63055655796343757, 11.49999999999999645 ) ) ;
#36455=CARTESIAN_POINT ( 'NONE',  ( -55.62287095715005592, -29.50247984919015209, -1.443849546365056913 ) ) ;
#36457=CARTESIAN_POINT ( 'NONE',  ( 18.07348078632662691, -10.09602009226539288, -1.500000000000002220 ) ) ;
#36459=EDGE_CURVE ( 'NONE', #32994, #28964, #66896, .T. ) ;
#36461=ORIENTED_EDGE ( 'NONE', *, *, #87194, .T. ) ;
#36462=CARTESIAN_POINT ( 'NONE',  ( -28.49465926560497309, -23.99116614675283543, -0.2315644524145782090 ) ) ;
#36463=ORIENTED_EDGE ( 'NONE', *, *, #54781, .T. ) ;
#36466=CARTESIAN_POINT ( 'NONE',  ( 11.32296221242833667, -17.63459971646239310, -1.500000000000002220 ) ) ;
#36467=CARTESIAN_POINT ( 'NONE',  ( -8.471812324360341151, -20.26817064352238162, 11.49999999999999645 ) ) ;
#36468=AXIS2_PLACEMENT_3D ( 'NONE', #2533, #24850, #71543 ) ;
#36470=CARTESIAN_POINT ( 'NONE',  ( -5.199590022849982063, -21.90925200621149571, -1.500000000000002220 ) ) ;
#36473=CARTESIAN_POINT ( 'NONE',  ( -17.07941033872765146, 12.18221932706078370, 11.49999999999998934 ) ) ;
#36475=CARTESIAN_POINT ( 'NONE',  ( -119.5886893414437679, -24.51419770103158768, 9.386484678747159194 ) ) ;
#36479=VERTEX_POINT ( 'NONE', #22099 ) ;
#36480=DIRECTION ( 'NONE',  ( -1.000000000000000000, -3.773278334444167608E-23, -8.201307833595939069E-29 ) ) ;
#36481=CARTESIAN_POINT ( 'NONE',  ( -18.34654256122676941, -11.15389649534839833, -1.500000000000002220 ) ) ;
#36483=ORIENTED_EDGE ( 'NONE', *, *, #94702, .F. ) ;
#36484=CARTESIAN_POINT ( 'NONE',  ( -13.65698368949537311, 16.12507722524849996, 11.49999999999998934 ) ) ;
#36486=CARTESIAN_POINT ( 'NONE',  ( -64.59767678124504187, -23.96119346886879953, -0.6495511937832134652 ) ) ;
#36489=CARTESIAN_POINT ( 'NONE',  ( -100.3562339080374102, -25.11078286826155193, 2.834876632948881259 ) ) ;
#36490=CARTESIAN_POINT ( 'NONE',  ( -21.57569705560537088, 4.917917830663471435, -1.500000000000002220 ) ) ;
#36491=CARTESIAN_POINT ( 'NONE',  ( -116.5517209740605864, -24.65952944569305316, 1.056160979905712338 ) ) ;
#36493=B_SPLINE_CURVE_WITH_KNOTS ( 'NONE', 3,
 ( #94783, #34894, #56749, #25270 ),
 .UNSPECIFIED., .F., .F.,
 ( 4, 4 ),
 ( 0.000000000000000000, 9.999999999998897304E-05 ),
 .UNSPECIFIED. ) ;
#36494=LINE ( 'NONE', #66971, #6020 ) ;
#36498=CARTESIAN_POINT ( 'NONE',  ( -18.22486019313910077, 6.713856318530649681, 11.49999999999998934 ) ) ;
#36499=CARTESIAN_POINT ( 'NONE',  ( -17.73838780825237649, 11.93509662624355450, -1.500000000000002220 ) ) ;
#36500=CARTESIAN_POINT ( 'NONE',  ( -26.29203710134576610, -24.90485257105619965, 6.397296682987914984 ) ) ;
#36501=DIRECTION ( 'NONE',  ( 1.000000000000000000, 3.773278334444166432E-23, 8.201307841325785021E-29 ) ) ;
#36503=CARTESIAN_POINT ( 'NONE',  ( -84.52287095715007581, -24.66019654487199730, 8.947790411086122830 ) ) ;
#36505=CARTESIAN_POINT ( 'NONE',  ( 20.10346781357453949, 10.43426432342431553, -1.500000000000002220 ) ) ;
#36507=CARTESIAN_POINT ( 'NONE',  ( -109.6228709571500559, -23.47593901973091235, -1.443836447538999312 ) ) ;
#36508=CARTESIAN_POINT ( 'NONE',  ( -104.5228709571500758, -24.64965694238407323, 8.947790433994194714 ) ) ;
#36509=CARTESIAN_POINT ( 'NONE',  ( -15.99800673754971037, 11.70972097625665675, 11.49999999999999645 ) ) ;
#36515=CARTESIAN_POINT ( 'NONE',  ( -29.81175120719462157, -25.26027006566499011, 4.942810958528816023 ) ) ;
#36517=CARTESIAN_POINT ( 'NONE',  ( 5.568959250215116619, -20.88136358707659923, 11.49999999999998934 ) ) ;
#36518=CARTESIAN_POINT ( 'NONE',  ( -26.89577987079026045, -24.79392825080098461, 7.339462090957008300 ) ) ;
#36519=CARTESIAN_POINT ( 'NONE',  ( 17.07123823605233781, 9.195568589125342029, -1.500000000000002220 ) ) ;
#36520=ADVANCED_FACE ( 'NONE', ( #30727 ), #25615, .T. ) ;
#36522=CARTESIAN_POINT ( 'NONE',  ( -35.62287095715006302, -24.63287334234179227, 0.9662140553045417413 ) ) ;
#36523=CARTESIAN_POINT ( 'NONE',  ( -19.37706247964952411, -4.161318200553020041, 11.49999999999998934 ) ) ;
#36525=CARTESIAN_POINT ( 'NONE',  ( 20.34676669208793953, -0.1217515720461415790, 11.49999999999999645 ) ) ;
#36526=CARTESIAN_POINT ( 'NONE',  ( -119.5228709571500616, -24.66019654487200441, 8.947790411086108620 ) ) ;
#36530=ORIENTED_EDGE ( 'NONE', *, *, #95403, .F. ) ;
#36531=CARTESIAN_POINT ( 'NONE',  ( -102.5170194679072182, -23.96169478059713853, 10.65365249895717881 ) ) ;
#36533=CARTESIAN_POINT ( 'NONE',  ( -44.62287095715006302, -23.96127896941632685, -0.6493128931037885909 ) ) ;
#36536=CARTESIAN_POINT ( 'NONE',  ( -87.22287095715006444, -23.47596703998600631, 11.44779298504227860 ) ) ;
#36537=CARTESIAN_POINT ( 'NONE',  ( -1.290058840521481454, 20.04182742388497473, 11.49999999999998934 ) ) ;
#36539=LINE ( 'NONE', #46161, #69421 ) ;
#36540=VERTEX_POINT ( 'NONE', #15987 ) ;
#36542=CARTESIAN_POINT ( 'NONE',  ( -21.19308438721250099, -8.479022899233653376, 11.49999999999999645 ) ) ;
#36544=CARTESIAN_POINT ( 'NONE',  ( -86.62287095715005592, -24.50216790748099527, 0.6166512839513639266 ) ) ;
#36547=DIRECTION ( 'NONE',  ( 3.773278334444167608E-23, -1.000000000000000000, 0.000000000000000000 ) ) ;
#36548=EDGE_CURVE ( 'NONE', #16850, #17644, #8386, .T. ) ;
#36549=CARTESIAN_POINT ( 'NONE',  ( -19.61019785865472542, -10.87575402790796453, 11.49999999999999645 ) ) ;
#36550=CARTESIAN_POINT ( 'NONE',  ( -98.87749449787162348, -25.03707831087709934, 7.590867751134624974 ) ) ;
#36552=CARTESIAN_POINT ( 'NONE',  ( 20.27773211485958527, -1.686570798567030183, 11.49999999999998934 ) ) ;
#36553=ORIENTED_EDGE ( 'NONE', *, *, #23466, .F. ) ;
#36554=CARTESIAN_POINT ( 'NONE',  ( -11.38079350637645959, -19.95400817559217899, 11.49999999999998934 ) ) ;
#36555=CARTESIAN_POINT ( 'NONE',  ( -37.58953762381673158, -24.65952944569304606, 1.056160979905692798 ) ) ;
#36556=ORIENTED_EDGE ( 'NONE', *, *, #19698, .T. ) ;
#36559=LINE ( 'NONE', #74624, #1048 ) ;
#36560=CARTESIAN_POINT ( 'NONE',  ( -8.014198274750887308, -19.69740135394370384, 11.49999999999999645 ) ) ;
#36561=VERTEX_POINT ( 'NONE', #33730 ) ;
#36563=B_SPLINE_CURVE_WITH_KNOTS ( 'NONE', 3,
 ( #31412, #456, #78066, #24790, #92303, #47651 ),
 .UNSPECIFIED., .F., .F.,
 ( 4, 2, 4 ),
 ( 0.000000000000000000, 0.001381645784125716319, 0.002763291568251432639 ),
 .UNSPECIFIED. ) ;
#36565=CARTESIAN_POINT ( 'NONE',  ( -19.05511597014879044, -11.33806725510066826, 11.49999999999998934 ) ) ;
#36566=CARTESIAN_POINT ( 'NONE',  ( -3.087264924507187924, 20.40197043678811539, -1.500000000000002220 ) ) ;
#36572=ORIENTED_EDGE ( 'NONE', *, *, #34205, .F. ) ;
#36573=EDGE_CURVE ( 'NONE', #38454, #77746, #58450, .T. ) ;
#36574=EDGE_LOOP ( 'NONE', ( #50858, #85009, #332, #4550 ) ) ;
#36578=CARTESIAN_POINT ( 'NONE',  ( -20.76960556195881225, -0.3855258213679747525, -1.500000000000002220 ) ) ;
#36579=CARTESIAN_POINT ( 'NONE',  ( 1.329761939549756855, 21.69843865049760367, 11.49999999999999645 ) ) ;
#36580=EDGE_LOOP ( 'NONE', ( #9631, #35102, #1625, #74228 ) ) ;
#36581=CARTESIAN_POINT ( 'NONE',  ( -40.52227049441191298, -25.31583770613250195, 5.079412502965257481 ) ) ;
#36583=CARTESIAN_POINT ( 'NONE',  ( -115.6250729497555909, -24.73486907724917927, 1.287355809206966573 ) ) ;
#36584=CARTESIAN_POINT ( 'NONE',  ( 15.48037617655995923, 16.25473645317415361, 11.49999999999998934 ) ) ;
#36587=CARTESIAN_POINT ( 'NONE',  ( -51.22891850606554698, -25.26334649059542059, 4.264007109377201843 ) ) ;
#36589=B_SPLINE_CURVE_WITH_KNOTS ( 'NONE', 3,
 ( #56733, #10533, #57236, #2433 ),
 .UNSPECIFIED., .F., .F.,
 ( 4, 4 ),
 ( 0.000000000000000000, 9.999999999998897304E-05 ),
 .UNSPECIFIED. ) ;
#36590=CARTESIAN_POINT ( 'NONE',  ( -75.52287095715006160, -24.99132157543084176, 2.256160258750667502 ) ) ;
#36593=ORIENTED_EDGE ( 'NONE', *, *, #18741, .F. ) ;
#36594=VERTEX_POINT ( 'NONE', #18001 ) ;
#36595=DIRECTION ( 'NONE',  ( -1.000000000000000000, -3.773278334444167608E-23, -8.201307833595939069E-29 ) ) ;
#36598=CARTESIAN_POINT ( 'NONE',  ( 1.434216325579209750, -21.26356369375713484, -1.500000000000002220 ) ) ;
#36600=CARTESIAN_POINT ( 'NONE',  ( -80.58953762381671027, -25.00182538069145366, 7.747789668545099317 ) ) ;
#36602=CARTESIAN_POINT ( 'NONE',  ( -17.33045254171255678, -11.89390297951003816, -1.500000000000002220 ) ) ;
#36604=CARTESIAN_POINT ( 'NONE',  ( 17.32531159343115945, 14.66459048539768162, 11.49999999999998934 ) ) ;
#36605=CARTESIAN_POINT ( 'NONE',  ( -99.53443088461749255, -25.25502385701537023, 3.893674835496924391 ) ) ;
#36607=FACE_OUTER_BOUND ( 'NONE', #86859, .T. ) ;
#36608=CARTESIAN_POINT ( 'NONE',  ( -3.478157889954244464, -21.63767827151469447, -1.500000000000002220 ) ) ;
#36609=DIRECTION ( 'NONE',  ( 0.000000000000000000, -2.173523156925980399E-06, 0.9999999999976378895 ) ) ;
#36611=CARTESIAN_POINT ( 'NONE',  ( -40.49165087243459737, -25.29352311369862605, 5.543942880681965946 ) ) ;
#36613=VECTOR ( 'NONE', #29386, 1000.000000000000114 ) ;
#36614=AXIS2_PLACEMENT_3D ( 'NONE', #32809, #64287, #70883 ) ;
#36615=ORIENTED_EDGE ( 'NONE', *, *, #52069, .F. ) ;
#36616=CARTESIAN_POINT ( 'NONE',  ( -120.5228709571500900, -24.82558206586149652, 1.605769216559630008 ) ) ;
#36618=CARTESIAN_POINT ( 'NONE',  ( -20.42273151058504510, -23.87832360206071769, 1.095224832288504091 ) ) ;
#36619=CARTESIAN_POINT ( 'NONE',  ( 17.81766572339076404, -11.58780717566545526, 11.49999999999998934 ) ) ;
#36620=CARTESIAN_POINT ( 'NONE',  ( -112.5161646695722766, -24.34968618360934656, 0.1864209137779000991 ) ) ;
#36621=CARTESIAN_POINT ( 'NONE',  ( -26.09636659181000695, -24.97064981342374423, 4.940287549563596059 ) ) ;
#36622=EDGE_CURVE ( 'NONE', #21715, #70027, #78906, .T. ) ;
#36623=CARTESIAN_POINT ( 'NONE',  ( -85.63412233528902107, -24.40034930558991633, 0.3402023900116044608 ) ) ;
#36624=CARTESIAN_POINT ( 'NONE',  ( -33.56120742164601722, -23.73766607897670866, -1.055555164236444687 ) ) ;
#36626=DIRECTION ( 'NONE',  ( -3.773278334453079618E-23, 0.9999999999976377785, 2.173523156925979975E-06 ) ) ;
#36627=ORIENTED_EDGE ( 'NONE', *, *, #97429, .F. ) ;
#36628=DIRECTION ( 'NONE',  ( -3.773278334444167608E-23, 1.000000000000000000, 0.000000000000000000 ) ) ;
#36629=CARTESIAN_POINT ( 'NONE',  ( 18.19143915067776263, 7.407926943018095400, 11.49999999999999645 ) ) ;
#36631=CARTESIAN_POINT ( 'NONE',  ( -100.6228709571500559, -24.99156045073393173, 7.747789690856161648 ) ) ;
#36633=EDGE_CURVE ( 'NONE', #66681, #2671, #53398, .T. ) ;
#36634=CARTESIAN_POINT ( 'NONE',  ( -88.62358605409035306, -24.66019654487199730, 8.947790411086115725 ) ) ;
#36635=CARTESIAN_POINT ( 'NONE',  ( -99.45104055277701605, -25.31439635812596478, 5.670438249640629813 ) ) ;
#36636=CARTESIAN_POINT ( 'NONE',  ( -25.78296037513418781, -24.81720370909834017, 6.769897328156279315 ) ) ;
#36637=EDGE_CURVE ( 'NONE', #38812, #68323, #89701, .T. ) ;
#36639=CARTESIAN_POINT ( 'NONE',  ( -16.05533900033903549, 11.45903963230415101, 11.49999999999998934 ) ) ;
#36641=ORIENTED_EDGE ( 'NONE', *, *, #50274, .F. ) ;
#36643=CARTESIAN_POINT ( 'NONE',  ( -70.62287095715009855, -24.83602698348160587, 1.605859176311266845 ) ) ;
#36644=B_SPLINE_CURVE_WITH_KNOTS ( 'NONE', 3,
 ( #63991, #72584, #62463, #16277 ),
 .UNSPECIFIED., .F., .F.,
 ( 4, 4 ),
 ( 0.000000000000000000, 0.0001000000000000098033 ),
 .UNSPECIFIED. ) ;
#36647=EDGE_CURVE ( 'NONE', #97579, #28117, #87008, .T. ) ;
#36648=ORIENTED_EDGE ( 'NONE', *, *, #24445, .F. ) ;
#36650=CARTESIAN_POINT ( 'NONE',  ( -69.58953762381672448, -24.66019654487198665, 8.947790411086131712 ) ) ;
#36651=CARTESIAN_POINT ( 'NONE',  ( -55.53128016475043438, -24.83618233451448987, 1.606449574219538379 ) ) ;
#36652=DIRECTION ( 'NONE',  ( 3.773278334444166432E-23, -1.000000000000000000, 0.000000000000000000 ) ) ;
#36656=CARTESIAN_POINT ( 'NONE',  ( 6.038693664686949347, 19.05185810397003721, -1.500000000000002220 ) ) ;
#36658=CARTESIAN_POINT ( 'NONE',  ( -0.07101499051468204704, -22.13065514132824418, 9.689530304921902371 ) ) ;
#36660=CARTESIAN_POINT ( 'NONE',  ( -63.52287095715004739, -23.47593901973090169, -1.443836447538996870 ) ) ;
#36665=CARTESIAN_POINT ( 'NONE',  ( -28.62287095715004881, -24.49608681932686949, 1.056161686216224860 ) ) ;
#36666=CARTESIAN_POINT ( 'NONE',  ( -39.56088500995654300, -23.73766607897669800, -1.055555164236461341 ) ) ;
#36667=CARTESIAN_POINT ( 'NONE',  ( -101.5468792378191836, -25.25287247409163527, 6.236250661346386615 ) ) ;
#36668=CARTESIAN_POINT ( 'NONE',  ( -51.66173670239771099, -25.26279960158665006, 4.265171648276663063 ) ) ;
#36670=EDGE_LOOP ( 'NONE', ( #47857, #21973, #72557, #10414 ) ) ;
#36671=DIRECTION ( 'NONE',  ( 3.773278334444166432E-23, -1.000000000000000000, 0.000000000000000000 ) ) ;
#36672=DIRECTION ( 'NONE',  ( -3.773278334453079030E-23, 0.9999999999976377785, 2.173523156925979128E-06 ) ) ;
#36673=AXIS2_PLACEMENT_3D ( 'NONE', #52187, #76997, #76002 ) ;
#36674=ORIENTED_EDGE ( 'NONE', *, *, #547, .T. ) ;
#36675=VECTOR ( 'NONE', #88508, 1000.000000000000114 ) ;
#36676=CARTESIAN_POINT ( 'NONE',  ( -15.67655817637044890, 12.86142704545212290, 11.49999999999998934 ) ) ;
#36677=CARTESIAN_POINT ( 'NONE',  ( -122.5572046973127698, -23.48783264082477373, -1.443836473390087471 ) ) ;
#36678=PLANE ( 'NONE',  #92281 ) ;
#36682=B_SPLINE_CURVE_WITH_KNOTS ( 'NONE', 3,
 ( #30165, #92066, #14936, #46899, #69739, #17441 ),
 .UNSPECIFIED., .F., .F.,
 ( 4, 2, 4 ),
 ( 0.000000000000000000, 0.001380764517854760846, 0.002761529035709521691 ),
 .UNSPECIFIED. ) ;
#36683=ORIENTED_EDGE ( 'NONE', *, *, #69005, .T. ) ;
#36684=CARTESIAN_POINT ( 'NONE',  ( -40.43756433397305727, -29.50248914370730091, 2.832395270851967073 ) ) ;
#36685=CARTESIAN_POINT ( 'NONE',  ( -46.52287095715006160, -24.64965694238406613, 8.947790433994203596 ) ) ;
#36686=CARTESIAN_POINT ( 'NONE',  ( 16.02535498940104830, 12.03463022438520191, -1.500000000000002220 ) ) ;
#36687=CARTESIAN_POINT ( 'NONE',  ( 16.98782256641479904, -12.52229676876588371, 11.49999999999999645 ) ) ;
#36688=CARTESIAN_POINT ( 'NONE',  ( -28.37365055580376350, -24.90401935843307157, 7.412184485816843527 ) ) ;
#36690=CARTESIAN_POINT ( 'NONE',  ( 7.254013858510784729, 20.86747967231135803, 11.49999999999998934 ) ) ;
#36691=CARTESIAN_POINT ( 'NONE',  ( 7.908618202329199320, -18.92053725880622039, 11.49999999999998934 ) ) ;
#36692=CARTESIAN_POINT ( 'NONE',  ( -36.62287095715005592, -29.50248528299804818, 1.056150453629031594 ) ) ;
#36695=LINE ( 'NONE', #69135, #55773 ) ;
#36698=CARTESIAN_POINT ( 'NONE',  ( -67.62287095715004170, -23.95044443724991368, 10.65354141964649592 ) ) ;
#36699=EDGE_CURVE ( 'NONE', #57603, #57780, #86093, .T. ) ;
#36700=EDGE_LOOP ( 'NONE', ( #68101, #60067, #19069, #5507 ) ) ;
#36702=CARTESIAN_POINT ( 'NONE',  ( -54.62287095715005592, -29.50248528299804818, 1.056150453629033370 ) ) ;
#36703=CARTESIAN_POINT ( 'NONE',  ( -127.6228709571500559, -24.64965695001469115, 8.947790433994173398 ) ) ;
#36704=CARTESIAN_POINT ( 'NONE',  ( -62.22287095715002891, -23.47593901973090524, -1.443836447538997758 ) ) ;
#36705=CARTESIAN_POINT ( 'NONE',  ( -18.72588118538106272, -8.511115862834014223, -1.500000000000002220 ) ) ;
#36707=CARTESIAN_POINT ( 'NONE',  ( 4.075586527997184128, 21.15050231453075824, 11.49999999999999645 ) ) ;
#36708=ORIENTED_EDGE ( 'NONE', *, *, #52048, .F. ) ;
#36709=PLANE ( 'NONE',  #59647 ) ;
#36710=AXIS2_PLACEMENT_3D ( 'NONE', #84622, #62304, #46572 ) ;
#36711=PLANE ( 'NONE',  #59360 ) ;
#36712=CARTESIAN_POINT ( 'NONE',  ( 5.437191932089902480, -21.69250089042843754, -1.500000000000002220 ) ) ;
#36713=EDGE_CURVE ( 'NONE', #29762, #7487, #44961, .T. ) ;
#36714=ADVANCED_FACE ( 'NONE', ( #89510 ), #41858, .T. ) ;
#36715=DIRECTION ( 'NONE',  ( -3.773278334453079030E-23, 0.9999999999976377785, 2.173523156925979128E-06 ) ) ;
#36719=FACE_OUTER_BOUND ( 'NONE', #97592, .T. ) ;
#36720=ADVANCED_FACE ( 'NONE', ( #51454 ), #88019, .T. ) ;
#36721=CARTESIAN_POINT ( 'NONE',  ( 20.89859092893058801, 0.06103081833375877813, -1.500000000000002220 ) ) ;
#36722=VERTEX_POINT ( 'NONE', #65210 ) ;
#36723=CARTESIAN_POINT ( 'NONE',  ( -86.62887871871048162, -24.34968618360933945, 0.1864209137778916059 ) ) ;
#36726=CARTESIAN_POINT ( 'NONE',  ( -32.62287095715004881, -29.50247984919015209, -1.443849546365062242 ) ) ;
#36727=CARTESIAN_POINT ( 'NONE',  ( 5.994809752082427501, 20.21905721239408393, -1.500000000000002220 ) ) ;
#36729=CARTESIAN_POINT ( 'NONE',  ( -117.5188432126315519, -24.15543982623907837, -0.2315651400026547124 ) ) ;
#36731=DIRECTION ( 'NONE',  ( -3.773278334453079618E-23, 0.9999999999976377785, 2.173523156925979975E-06 ) ) ;
#36732=CARTESIAN_POINT ( 'NONE',  ( -90.62287095715004170, -23.47596703998600631, 11.44779298504227860 ) ) ;
#36734=CARTESIAN_POINT ( 'NONE',  ( -16.40380107638378604, 14.33077157581830008, -1.500000000000002220 ) ) ;
#36735=CARTESIAN_POINT ( 'NONE',  ( -71.33541886227440898, -25.24674103807599934, 5.089068620786424191 ) ) ;
#36736=CARTESIAN_POINT ( 'NONE',  ( 4.546662993595487201, 21.82331882591909178, 11.49999999999999645 ) ) ;
#36737=ORIENTED_EDGE ( 'NONE', *, *, #8683, .T. ) ;
#36738=CARTESIAN_POINT ( 'NONE',  ( -53.62287095715005592, -24.64965695001467694, 8.947790433994185832 ) ) ;
#36739=CARTESIAN_POINT ( 'NONE',  ( -92.58953762381672448, -23.47596703998600631, 11.44779298504227683 ) ) ;
#36741=DIRECTION ( 'NONE',  ( 0.000000000000000000, -0.9999999999976377785, -2.173523156925979975E-06 ) ) ;
#36744=EDGE_LOOP ( 'NONE', ( #30571, #29474, #40239, #11122 ) ) ;
#36746=ORIENTED_EDGE ( 'NONE', *, *, #97076, .T. ) ;
#36747=CARTESIAN_POINT ( 'NONE',  ( -100.9686692281476610, -25.15033489556367741, 7.001233543541374615 ) ) ;
#36751=DIRECTION ( 'NONE',  ( -3.773278334453079618E-23, 0.9999999999976377785, 2.173523156925979975E-06 ) ) ;
#36753=CARTESIAN_POINT ( 'NONE',  ( -9.862393454161701101, 16.67994275214481092, 11.49999999999998934 ) ) ;
#36755=ORIENTED_EDGE ( 'NONE', *, *, #63672, .F. ) ;
#36757=CARTESIAN_POINT ( 'NONE',  ( -0.1161231997828221785, -19.40653004597026410, 11.49999999999999645 ) ) ;
#36764=AXIS2_PLACEMENT_3D ( 'NONE', #86792, #78165, #25900 ) ;
#36766=ADVANCED_FACE ( 'NONE', ( #81900 ), #33603, .T. ) ;
#36767=CARTESIAN_POINT ( 'NONE',  ( 13.00645856128228495, 14.71372164842801844, 11.49999999999998934 ) ) ;
#36768=DIRECTION ( 'NONE',  ( 0.000000000000000000, -0.9999999999976377785, -2.173523156925979975E-06 ) ) ;
#36770=CARTESIAN_POINT ( 'NONE',  ( -13.10987527212420645, -17.12674121770768920, 11.49999999999998934 ) ) ;
#36772=PLANE ( 'NONE',  #52973 ) ;
#36773=CARTESIAN_POINT ( 'NONE',  ( -114.6228709571500559, -29.50250243563736774, 8.947779886222136270 ) ) ;
#36774=EDGE_CURVE ( 'NONE', #16634, #46870, #44346, .T. ) ;
#36776=CARTESIAN_POINT ( 'NONE',  ( -21.48638390452810043, -8.140844714011898020, -1.500000000000002220 ) ) ;
#36778=CARTESIAN_POINT ( 'NONE',  ( -89.40841769935769889, -25.27880950044345809, 5.947789066509453271 ) ) ;
#36779=DIRECTION ( 'NONE',  ( -3.773278334453079618E-23, 0.9999999999976377785, 2.173523156925979975E-06 ) ) ;
#36780=CARTESIAN_POINT ( 'NONE',  ( 1.109688723463823301, -20.12803150795971874, 11.49999999999999645 ) ) ;
#36781=CARTESIAN_POINT ( 'NONE',  ( -45.62287095715005592, -23.84081130438200091, 10.88220057463249013 ) ) ;
#36782=DIRECTION ( 'NONE',  ( 0.000000000000000000, -0.9999999999976377785, -2.173523156925979128E-06 ) ) ;
#36783=FACE_OUTER_BOUND ( 'NONE', #37547, .T. ) ;
#36784=CARTESIAN_POINT ( 'NONE',  ( -29.52287095715006160, -23.40102634903646717, 11.44779303447556629 ) ) ;
#36785=CARTESIAN_POINT ( 'NONE',  ( -110.9796143976588070, -25.29779200634336078, 3.502226275253062848 ) ) ;
#36786=EDGE_CURVE ( 'NONE', #16750, #79871, #49819, .T. ) ;
#36787=CARTESIAN_POINT ( 'NONE',  ( -1.769646468872753120, 19.80360307839763934, -1.500000000000002220 ) ) ;
#36788=CARTESIAN_POINT ( 'NONE',  ( -47.52287095715004739, -24.66019654487199375, 8.947790411086122830 ) ) ;
#36789=CARTESIAN_POINT ( 'NONE',  ( -0.9724026449420489771, -19.73431249065222204, -1.500000000000002220 ) ) ;
#36791=CARTESIAN_POINT ( 'NONE',  ( -42.52916115802615593, -24.65952944569304606, 1.056160979905694353 ) ) ;
#36792=B_SPLINE_CURVE_WITH_KNOTS ( 'NONE', 3,
 ( #70946, #69438, #62335, #47610, #54725, #927 ),
 .UNSPECIFIED., .F., .F.,
 ( 4, 2, 4 ),
 ( 0.000000000000000000, 0.001380901958385389412, 0.002761803916770778824 ),
 .UNSPECIFIED. ) ;
#36793=CARTESIAN_POINT ( 'NONE',  ( -73.52287095715007581, -23.47596703998600631, 11.44779298504228748 ) ) ;
#36795=CARTESIAN_POINT ( 'NONE',  ( 20.27745880512110688, -4.159726151199424571, 11.49999999999999645 ) ) ;
#36797=CARTESIAN_POINT ( 'NONE',  ( -111.5562042904833788, -24.64965694238575367, 8.947790433994185832 ) ) ;
#36799=CARTESIAN_POINT ( 'NONE',  ( -50.15966858932511485, -25.31439280820845283, 5.214258294773329361 ) ) ;
#36800=CARTESIAN_POINT ( 'NONE',  ( 18.72737137862276313, -12.84423604280260278, 11.49999999999999645 ) ) ;
#36801=VERTEX_POINT ( 'NONE', #29099 ) ;
#36802=B_SPLINE_SURFACE_WITH_KNOTS ( 'NONE', 3, 3, ( 
 ( #85423, #8307, #15908, #46875 ),
 ( #77795, #39250, #70210, #31636 ),
 ( #62607, #15408, #46369, #7296 ),
 ( #78304, #93528, #8812, #77302 ),
 ( #24022, #69207, #16405, #39748 ),
 ( #70708, #32137, #94540, #7803 ),
 ( #84427, #45879, #100122, #1206 ) ),
 .UNSPECIFIED., .F., .F., .F.,
 ( 4, 3, 4 ),
 ( 4, 4 ),
 ( 0.7945040050992232539, 0.8970133687736495665, 0.9995227324480758790 ),
 ( 0.3695879146558129213, 0.3707712655177336503 ),
 .UNSPECIFIED. ) ;
#36805=CARTESIAN_POINT ( 'NONE',  ( -20.16912494768211417, -0.3064379698199363733, 11.49999999999998934 ) ) ;
#36806=CARTESIAN_POINT ( 'NONE',  ( -63.54869588136745051, -24.15543982623906416, -0.2315651400026651485 ) ) ;
#36812=CARTESIAN_POINT ( 'NONE',  ( 20.41593879258296695, -10.28030303932802880, 11.49999999999998934 ) ) ;
#36813=CARTESIAN_POINT ( 'NONE',  ( -74.62287095715005592, -23.48783264082478794, -1.443836473390067265 ) ) ;
#36814=B_SPLINE_CURVE_WITH_KNOTS ( 'NONE', 3,
 ( #426, #77539, #39993, #31378, #62342, #38496 ),
 .UNSPECIFIED., .F., .F.,
 ( 4, 2, 4 ),
 ( 6.391158118977072634E-06, 0.001387004593080798072, 0.002767618028042619343 ),
 .UNSPECIFIED. ) ;
#36815=CARTESIAN_POINT ( 'NONE',  ( -10.34410514300256523, -18.92461576200269491, -1.500000000000002220 ) ) ;
#36816=CARTESIAN_POINT ( 'NONE',  ( -123.5911763806425796, -23.73766607897670866, -1.055555164236449350 ) ) ;
#36817=DIRECTION ( 'NONE',  ( -3.773278334444167608E-23, 1.000000000000000000, 0.000000000000000000 ) ) ;
#36818=CARTESIAN_POINT ( 'NONE',  ( 21.27769986149581172, 7.469961712261545372, 11.49999999999999645 ) ) ;
#36820=CARTESIAN_POINT ( 'NONE',  ( -69.87926231432713564, -25.31612431666963303, 4.903252905761131153 ) ) ;
#36821=CARTESIAN_POINT ( 'NONE',  ( 19.14557405504459453, -10.84957060938160289, -1.500000000000002220 ) ) ;
#36822=LINE ( 'NONE', #92584, #78665 ) ;
#36823=CARTESIAN_POINT ( 'NONE',  ( -41.32330479122543210, -25.29087095761961379, 3.114706565199032440 ) ) ;
#36824=ORIENTED_EDGE ( 'NONE', *, *, #31089, .T. ) ;
#36826=ADVANCED_FACE ( 'NONE', ( #52450 ), #76705, .T. ) ;
#36829=CARTESIAN_POINT ( 'NONE',  ( -77.62287095715005592, -24.50216790748097040, 0.6166512839513687005 ) ) ;
#36830=EDGE_CURVE ( 'NONE', #63682, #17879, #30383, .T. ) ;
#36833=EDGE_CURVE ( 'NONE', #33400, #11110, #58262, .T. ) ;
#36834=B_SPLINE_CURVE_WITH_KNOTS ( 'NONE', 3,
 ( #19923, #4712, #44277, #81335 ),
 .UNSPECIFIED., .F., .F.,
 ( 4, 4 ),
 ( 0.5391559877274726409, 0.5401567347682382225 ),
 .UNSPECIFIED. ) ;
#36835=ORIENTED_EDGE ( 'NONE', *, *, #33461, .F. ) ;
#36836=CARTESIAN_POINT ( 'NONE',  ( -81.52287095715010423, -23.48783264083388289, -1.443836473375922580 ) ) ;
#36837=FACE_OUTER_BOUND ( 'NONE', #86514, .T. ) ;
#36838=CARTESIAN_POINT ( 'NONE',  ( -104.5221999606295924, -23.48786465467241413, 11.44779295918254469 ) ) ;
#36839=CARTESIAN_POINT ( 'NONE',  ( 15.56926775127050000, -13.18612581554039132, -1.500000000000002220 ) ) ;
#36840=EDGE_CURVE ( 'NONE', #90955, #76106, #54657, .T. ) ;
#36844=EDGE_CURVE ( 'NONE', #27379, #32345, #41364, .T. ) ;
#36847=ORIENTED_EDGE ( 'NONE', *, *, #43126, .T. ) ;
#36848=CARTESIAN_POINT ( 'NONE',  ( -100.2228709571500644, -23.47596703998600631, 11.44779298504227860 ) ) ;
#36849=CARTESIAN_POINT ( 'NONE',  ( -97.52287095715003318, -24.66019654487200441, 8.947790411086119278 ) ) ;
#36850=CARTESIAN_POINT ( 'NONE',  ( 16.81283763619640936, 12.23492182941471107, -1.500000000000002220 ) ) ;
#36852=CARTESIAN_POINT ( 'NONE',  ( -54.62287095715005592, -24.64898659630528854, 1.056161002820821038 ) ) ;
#36856=ORIENTED_EDGE ( 'NONE', *, *, #18741, .T. ) ;
#36857=CARTESIAN_POINT ( 'NONE',  ( -73.62287095715005592, -29.50250243563736774, 8.947779886222143375 ) ) ;
#36858=CARTESIAN_POINT ( 'NONE',  ( -116.4728709571500360, -25.30558663486635140, 5.000950659935019971 ) ) ;
#36859=CARTESIAN_POINT ( 'NONE',  ( -86.52287095715006160, -23.47593901973090169, -1.443836447538996648 ) ) ;
#36861=CARTESIAN_POINT ( 'NONE',  ( 15.99899278244174639, -15.33069297701436184, 11.49999999999999645 ) ) ;
#36862=ORIENTED_EDGE ( 'NONE', *, *, #21702, .F. ) ;
#36863=CARTESIAN_POINT ( 'NONE',  ( -108.5519315939779830, -24.34968618360934656, 0.1864209137778971292 ) ) ;
#36864=CARTESIAN_POINT ( 'NONE',  ( -14.08738070862771963, 17.71811851510361535, -1.500000000000002220 ) ) ;
#36865=VECTOR ( 'NONE', #41865, 1000.000000000000114 ) ;
#36866=PLANE ( 'NONE',  #34430 ) ;
#36871=CARTESIAN_POINT ( 'NONE',  ( -15.22981678846565856, -13.14137338692033907, 11.49999999999998934 ) ) ;
#36872=CARTESIAN_POINT ( 'NONE',  ( -0.1490770655183801252, -21.12008023607309681, -1.443836447538997758 ) ) ;
#36875=CARTESIAN_POINT ( 'NONE',  ( 4.546662993595487201, 21.82331882591909178, -1.500000000000002220 ) ) ;
#36876=ORIENTED_EDGE ( 'NONE', *, *, #73065, .F. ) ;
#36877=CARTESIAN_POINT ( 'NONE',  ( -73.62287095715007013, -23.47596703998600276, 11.44779298504227860 ) ) ;
#36878=PLANE ( 'NONE',  #89683 ) ;
#36880=B_SPLINE_CURVE_WITH_KNOTS ( 'NONE', 3,
 ( #44021, #59257, #97805, #18319, #40662, #18809, #88335, #33043 ),
 .UNSPECIFIED., .F., .F.,
 ( 4, 2, 2, 4 ),
 ( -0.001224873891641419356, -0.0002244903592271048094, 0.0007758931731872097375, 0.002776660238015834711 ),
 .UNSPECIFIED. ) ;
#36882=CARTESIAN_POINT ( 'NONE',  ( 9.052818235119415746, 17.31195010612007223, -1.500000000000002220 ) ) ;
#36883=CARTESIAN_POINT ( 'NONE',  ( -19.99255411920323056, 7.849732829375159149, 11.49999999999998934 ) ) ;
#36885=CARTESIAN_POINT ( 'NONE',  ( -120.5228709571500616, -25.00158670708909625, 2.256160236439166411 ) ) ;
#36888=CARTESIAN_POINT ( 'NONE',  ( -9.359374538088376383, 20.77767741201286711, -1.500000000000002220 ) ) ;
#36892=CARTESIAN_POINT ( 'NONE',  ( -96.54754425073249990, -24.51419770103159834, 9.386484678747169852 ) ) ;
#36894=CARTESIAN_POINT ( 'NONE',  ( -19.95764006394758638, 0.7380318605572177004, 11.49999999999999645 ) ) ;
#36898=CARTESIAN_POINT ( 'NONE',  ( -44.22287095715006444, -23.47593901973090169, -1.443836447538997980 ) ) ;
#36900=CARTESIAN_POINT ( 'NONE',  ( -89.58953762381671027, -24.64898659630529210, 1.056161002820829031 ) ) ;
#36901=CARTESIAN_POINT ( 'NONE',  ( -124.5228709571500900, -23.48783264082477373, -1.443836473390085029 ) ) ;
#36902=CARTESIAN_POINT ( 'NONE',  ( 7.827691340095081607, 20.28360254610759839, -1.500000000000002220 ) ) ;
#36903=CARTESIAN_POINT ( 'NONE',  ( -40.62287095715005592, -29.50247984919015209, -1.443849546365060466 ) ) ;
#36904=CARTESIAN_POINT ( 'NONE',  ( -18.74126595726828626, 5.813943427813767606, -1.500000000000002220 ) ) ;
#36905=DIRECTION ( 'NONE',  ( 1.000000000000000000, 3.773278334444166432E-23, 8.201307841325785021E-29 ) ) ;
#36909=DIRECTION ( 'NONE',  ( -3.773278334453079030E-23, 0.9999999999976377785, 2.173523156925979128E-06 ) ) ;
#36910=CARTESIAN_POINT ( 'NONE',  ( -9.284664653622879626, 18.31210316397345395, 11.49999999999999645 ) ) ;
#36911=CARTESIAN_POINT ( 'NONE',  ( -50.24370449261476779, -25.30394787829096970, 5.202377319005417000 ) ) ;
#36912=DIRECTION ( 'NONE',  ( 0.000000000000000000, 0.9999999999976377785, 2.173523156925979128E-06 ) ) ;
#36913=B_SPLINE_CURVE_WITH_KNOTS ( 'NONE', 3,
 ( #97664, #90057, #20529, #51504 ),
 .UNSPECIFIED., .F., .F.,
 ( 4, 4 ),
 ( 0.000000000000000000, 9.999999999998897304E-05 ),
 .UNSPECIFIED. ) ;
#36914=ORIENTED_EDGE ( 'NONE', *, *, #67890, .F. ) ;
#36916=LINE ( 'NONE', #98809, #76928 ) ;
#36921=EDGE_CURVE ( 'NONE', #79917, #88666, #35256, .T. ) ;
#36922=CARTESIAN_POINT ( 'NONE',  ( 4.903590608199674072, 22.46510890469962263, 11.49999999999999645 ) ) ;
#36923=CARTESIAN_POINT ( 'NONE',  ( 0.9741843557120299923, -22.74547949729550922, 11.49999999999998934 ) ) ;
#36925=B_SPLINE_SURFACE_WITH_KNOTS ( 'NONE', 3, 3, ( 
 ( #1991, #94824, #70497, #982 ),
 ( #62903, #93828, #24314, #16698 ),
 ( #11581, #80598, #33933, #34431 ),
 ( #25818, #20187, #73488, #56788 ),
 ( #2995, #65906, #26815, #18205 ),
 ( #64912, #64411, #58279, #50657 ),
 ( #50164, #42559, #2490, #3986 ) ),
 .UNSPECIFIED., .F., .F., .F.,
 ( 4, 3, 4 ),
 ( 4, 4 ),
 ( 0.0004766839783820627473, 0.1029713700210898447, 0.2054660560637976141 ),
 ( 0.2095473025018212698, 0.2106567117982014459 ),
 .UNSPECIFIED. ) ;
#36926=LINE ( 'NONE', #51664, #2641 ) ;
#36927=CARTESIAN_POINT ( 'NONE',  ( -120.5228709571500616, -24.91570333825770689, 8.075032458260345436 ) ) ;
#36930=CARTESIAN_POINT ( 'NONE',  ( 13.84421170697429737, -16.98027460053469895, -1.500000000000002220 ) ) ;
#36932=CARTESIAN_POINT ( 'NONE',  ( -87.59864960828673475, -23.73791477778911840, 11.05961554403170588 ) ) ;
#36933=CARTESIAN_POINT ( 'NONE',  ( -41.22828023510016493, -25.31356029329619517, 4.766479152052003343 ) ) ;
#36935=DIRECTION ( 'NONE',  ( 1.000000000000000000, 3.773278334444166432E-23, 8.201307841325785021E-29 ) ) ;
#36936=DIRECTION ( 'NONE',  ( -3.773278334453080206E-23, 0.9999999999976377785, 2.173523156925979975E-06 ) ) ;
#36937=ORIENTED_EDGE ( 'NONE', *, *, #40173, .F. ) ;
#36939=CARTESIAN_POINT ( 'NONE',  ( -2.750569593922542300, -20.27526743851804625, -1.500000000000002220 ) ) ;
#36940=ORIENTED_EDGE ( 'NONE', *, *, #72008, .T. ) ;
#36942=ORIENTED_EDGE ( 'NONE', *, *, #89211, .F. ) ;
#36944=CARTESIAN_POINT ( 'NONE',  ( 22.92345266703080142, -2.467471440992916154, 11.49999999999998934 ) ) ;
#36946=CARTESIAN_POINT ( 'NONE',  ( -9.609455416251792670, -17.83980533922896683, -1.500000000000002220 ) ) ;
#36949=CARTESIAN_POINT ( 'NONE',  ( -26.07746707516802331, -24.95785182683525605, 4.938174481708933250 ) ) ;
#36951=CARTESIAN_POINT ( 'NONE',  ( -37.62287095715005592, -29.50247984919015209, -1.443849546365060466 ) ) ;
#36952=EDGE_CURVE ( 'NONE', #50678, #100104, #32603, .T. ) ;
#36954=CARTESIAN_POINT ( 'NONE',  ( -70.61332773891285797, -23.48783264082477018, -1.443836473390095021 ) ) ;
#36955=CARTESIAN_POINT ( 'NONE',  ( -9.924231251898440576, -18.97836718215353713, 11.49999999999999645 ) ) ;
#36956=ORIENTED_EDGE ( 'NONE', *, *, #21904, .T. ) ;
#36957=CARTESIAN_POINT ( 'NONE',  ( -104.6228709571500559, -29.50250243563736774, 8.947779886222138046 ) ) ;
#36958=CARTESIAN_POINT ( 'NONE',  ( -41.66425029149441173, -23.48783264082477729, -1.443836473390075925 ) ) ;
#36959=ADVANCED_FACE ( 'NONE', ( #648 ), #85379, .F. ) ;
#36960=ORIENTED_EDGE ( 'NONE', *, *, #27057, .T. ) ;
#36961=EDGE_CURVE ( 'NONE', #90802, #67691, #63111, .T. ) ;
#36962=CARTESIAN_POINT ( 'NONE',  ( -20.55201672899488585, 2.666056886502145673, 11.49999999999998934 ) ) ;
#36965=FACE_OUTER_BOUND ( 'NONE', #67725, .T. ) ;
#36966=ORIENTED_EDGE ( 'NONE', *, *, #22200, .T. ) ;
#36967=CARTESIAN_POINT ( 'NONE',  ( -55.52287095715006160, -24.62285846331433703, 9.038163153548362416 ) ) ;
#36970=CARTESIAN_POINT ( 'NONE',  ( -11.62490142266122639, -17.50836435561060256, -1.500000000000002220 ) ) ;
#36972=CARTESIAN_POINT ( 'NONE',  ( 21.10488023177059347, -6.046698511884514460, 11.49999999999999645 ) ) ;
#36973=CARTESIAN_POINT ( 'NONE',  ( -73.52211514783047619, -23.48786465467241058, 11.44779295918254824 ) ) ;
#36974=CARTESIAN_POINT ( 'NONE',  ( 16.93931825803137414, 14.88162037096512158, -1.500000000000002220 ) ) ;
#36975=B_SPLINE_CURVE_WITH_KNOTS ( 'NONE', 3,
 ( #3911, #81021, #82016, #88140 ),
 .UNSPECIFIED., .F., .F.,
 ( 4, 4 ),
 ( 0.000000000000000000, 1.000000000000000000 ),
 .UNSPECIFIED. ) ;
#36976=CARTESIAN_POINT ( 'NONE',  ( -20.39251343623233836, 4.912230638944180328, 11.49999999999998934 ) ) ;
#36977=DIRECTION ( 'NONE',  ( 1.000000000000000000, 3.773278334444166432E-23, 8.201307841325785021E-29 ) ) ;
#36979=DIRECTION ( 'NONE',  ( 0.000000000000000000, 2.173523156925980399E-06, -0.9999999999976378895 ) ) ;
#36980=VERTEX_POINT ( 'NONE', #1664 ) ;
#36981=AXIS2_PLACEMENT_3D ( 'NONE', #83201, #4103, #43170 ) ;
#36982=EDGE_LOOP ( 'NONE', ( #28141, #973, #19186, #74412 ) ) ;
#36983=ORIENTED_EDGE ( 'NONE', *, *, #33976, .T. ) ;
#36984=CARTESIAN_POINT ( 'NONE',  ( -66.52209609814681812, -23.48783264082476308, -1.443836473390097463 ) ) ;
#36985=CARTESIAN_POINT ( 'NONE',  ( -10.32266838563235467, 18.89866041204108527, -1.500000000000002220 ) ) ;
#36986=DIRECTION ( 'NONE',  ( 0.000000000000000000, 0.9999999999976377785, 2.173523156925979128E-06 ) ) ;
#36987=EDGE_LOOP ( 'NONE', ( #39220, #61693, #2466, #61674 ) ) ;
#36988=CARTESIAN_POINT ( 'NONE',  ( -20.79277273739468512, 3.736189789763188607, 11.49999999999998934 ) ) ;
#36990=FACE_OUTER_BOUND ( 'NONE', #41613, .T. ) ;
#36991=CARTESIAN_POINT ( 'NONE',  ( -100.5228709571500758, -24.92579138211019441, 1.929029949965663127 ) ) ;
#36993=CARTESIAN_POINT ( 'NONE',  ( -123.5562042904834072, -23.48783264082478794, -1.443836473390058384 ) ) ;
#36994=CARTESIAN_POINT ( 'NONE',  ( -9.153499762860807465, 20.15527781828815534, -1.500000000000002220 ) ) ;
#36995=CARTESIAN_POINT ( 'NONE',  ( -30.47287095715008576, -23.47593902499770380, -1.441415665115638456 ) ) ;
#36996=ADVANCED_FACE ( 'NONE', ( #24981 ), #55956, .T. ) ;
#36999=CARTESIAN_POINT ( 'NONE',  ( -79.62287095715008434, -23.94994826722565762, -0.6494450866342735829 ) ) ;
#37000=CARTESIAN_POINT ( 'NONE',  ( -41.86878170341644534, -25.27955791706579092, 4.256748853647015274 ) ) ;
#37002=CARTESIAN_POINT ( 'NONE',  ( -97.52287095715006160, -24.64965694238575011, 8.947790433994194714 ) ) ;
#37003=B_SPLINE_CURVE_WITH_KNOTS ( 'NONE', 3,
 ( #75134, #99461, #37580, #29455 ),
 .UNSPECIFIED., .F., .F.,
 ( 4, 4 ),
 ( 0.7510362966358483661, 0.7600427279079640108 ),
 .UNSPECIFIED. ) ;
#37004=CARTESIAN_POINT ( 'NONE',  ( -13.34961138979462270, 14.11212085816309880, -1.500000000000002220 ) ) ;
#37005=CARTESIAN_POINT ( 'NONE',  ( 18.99370601119529312, 9.851043883551550806, 11.49999999999998934 ) ) ;
#37006=CARTESIAN_POINT ( 'NONE',  ( -69.22054176954050320, -25.14415006753612758, 7.039201735951476024 ) ) ;
#37007=CARTESIAN_POINT ( 'NONE',  ( -81.62287095715004170, -23.48786465467241058, 11.44779295918254647 ) ) ;
#37008=EDGE_CURVE ( 'NONE', #64821, #52058, #94538, .T. ) ;
#37009=CARTESIAN_POINT ( 'NONE',  ( -106.5895376238167245, -24.65952944569304961, 1.056160979905703678 ) ) ;
#37011=CARTESIAN_POINT ( 'NONE',  ( 18.27610663105864219, 13.37729726205769154, -1.500000000000002220 ) ) ;
#37012=B_SPLINE_SURFACE_WITH_KNOTS ( 'NONE', 3, 1, ( 
 ( #44130, #84175 ),
 ( #77056, #23266 ),
 ( #48134, #39005 ),
 ( #443, #79062 ),
 ( #32399, #9555 ),
 ( #93790, #93283 ),
 ( #31396, #78552 ),
 ( #23775, #46635 ),
 ( #54750, #24286 ),
 ( #15666, #8056 ),
 ( #86681, #1459 ),
 ( #62357, #69958 ),
 ( #15163, #16665 ),
 ( #85685, #16165 ),
 ( #47636, #69458 ) ),
 .UNSPECIFIED., .F., .F., .F.,
 ( 4, 1, 1, 1, 1, 1, 1, 1, 1, 1, 1, 1, 4 ),
 ( 2, 2 ),
 ( 0.000000000000000000, 0.1227119423657796193, 0.2396849640167788842, 0.3518158552560940455, 0.4637661328620885093, 0.5208177931608346523, 0.5794482914480051372, 0.6406041451203223769, 0.7052975118059877646, 0.7736338807131363238, 0.8446693818863779679, 0.9200565080211464686, 1.000000000000000000 ),
 ( 0.000000000000000000, 1.000000000000000000 ),
 .UNSPECIFIED. ) ;
#37013=EDGE_LOOP ( 'NONE', ( #76283, #22332, #71558, #76502, #4639, #97761, #76338, #95747, #86464, #23502 ) ) ;
#37014=EDGE_CURVE ( 'NONE', #76617, #9739, #86019, .T. ) ;
#37016=DIRECTION ( 'NONE',  ( 0.000000000000000000, -0.9999999999976377785, -2.173523156925979975E-06 ) ) ;
#37017=CARTESIAN_POINT ( 'NONE',  ( 13.37688099249405127, 14.58279310912311111, 11.49999999999999645 ) ) ;
#37019=B_SPLINE_CURVE_WITH_KNOTS ( 'NONE', 3,
 ( #74342, #36781, #91554, #98662, #68231, #75328, #91058, #99160 ),
 .UNSPECIFIED., .F., .F.,
 ( 4, 2, 2, 4 ),
 ( 0.000000000000000000, 0.002001079623178221925, 0.003001619434767334622, 0.004002159246356447320 ),
 .UNSPECIFIED. ) ;
#37021=CARTESIAN_POINT ( 'NONE',  ( -86.52287095715006160, -29.50248528299804818, 1.056150453629040253 ) ) ;
#37023=CARTESIAN_POINT ( 'NONE',  ( 7.043455336710909620, -20.48365140995157674, -1.500000000000002220 ) ) ;
#37024=CARTESIAN_POINT ( 'NONE',  ( -26.61588051278965850, -24.82222928824689134, 7.072807463452274845 ) ) ;
#37026=CARTESIAN_POINT ( 'NONE',  ( -12.45040968399260883, -14.89389333286084671, -1.500000000000002220 ) ) ;
#37027=CARTESIAN_POINT ( 'NONE',  ( -129.6228709571500701, -23.48786465467241769, 11.44779295918253581 ) ) ;
#37028=CARTESIAN_POINT ( 'NONE',  ( -82.62287095715004170, -24.35013146730203815, 9.818937971375111928 ) ) ;
#37029=CARTESIAN_POINT ( 'NONE',  ( 4.927431051831622000, -19.18327824014073357, 11.49999999999998934 ) ) ;
#37031=CARTESIAN_POINT ( 'NONE',  ( -18.18203184671642703, 9.085611141607108365, 11.49999999999999645 ) ) ;
#37032=DIRECTION ( 'NONE',  ( -3.773278334453079618E-23, 0.9999999999976377785, 2.173523156925979975E-06 ) ) ;
#37034=B_SPLINE_CURVE_WITH_KNOTS ( 'NONE', 3,
 ( #88526, #59083, #82398, #81412 ),
 .UNSPECIFIED., .F., .F.,
 ( 4, 4 ),
 ( 0.000000000000000000, 0.0001000000000000028644 ),
 .UNSPECIFIED. ) ;
#37039=VECTOR ( 'NONE', #83078, 1000.000000000000114 ) ;
#37040=CARTESIAN_POINT ( 'NONE',  ( -82.58953762381672448, -23.48786465467241413, 11.44779295918254647 ) ) ;
#37041=CARTESIAN_POINT ( 'NONE',  ( -49.62287095715004170, -23.47596703998600631, 11.44779298504227505 ) ) ;
#37042=CARTESIAN_POINT ( 'NONE',  ( -4.751880754313710042, -19.48972053015312866, 11.49999999999998934 ) ) ;
#37044=ORIENTED_EDGE ( 'NONE', *, *, #2474, .T. ) ;
#37046=VECTOR ( 'NONE', #79721, 1000.000000000000114 ) ;
#37047=CARTESIAN_POINT ( 'NONE',  ( 13.81544771398824345, -18.15223324129861382, 11.49999999999999645 ) ) ;
#37048=CARTESIAN_POINT ( 'NONE',  ( -49.76261995625480949, -25.26258836565245502, 4.511523319824253697 ) ) ;
#37051=CARTESIAN_POINT ( 'NONE',  ( -43.62287095715004881, -24.64965695001467694, 8.947790433994187609 ) ) ;
#37053=DIRECTION ( 'NONE',  ( -3.773278334453079618E-23, 0.9999999999976377785, 2.173523156925979975E-06 ) ) ;
#37055=CARTESIAN_POINT ( 'NONE',  ( 18.17922461840205983, -9.147185827878928421, -1.500000000000002220 ) ) ;
#37058=CARTESIAN_POINT ( 'NONE',  ( -1.334576548209915225, -22.92891363262047832, -1.500000000000002220 ) ) ;
#37059=CARTESIAN_POINT ( 'NONE',  ( -53.52287095715005449, -23.96177878511308634, 10.65340807706330217 ) ) ;
#37062=B_SPLINE_CURVE_WITH_KNOTS ( 'NONE', 3,
 ( #66360, #42518, #20151, #73955 ),
 .UNSPECIFIED., .F., .F.,
 ( 4, 4 ),
 ( 0.000000000000000000, 0.0001000000000000028644 ),
 .UNSPECIFIED. ) ;
#37064=B_SPLINE_CURVE_WITH_KNOTS ( 'NONE', 3,
 ( #83682, #6566, #92789, #37513 ),
 .UNSPECIFIED., .F., .F.,
 ( 4, 4 ),
 ( 0.000000000000000000, 0.0001000000000000722533 ),
 .UNSPECIFIED. ) ;
#37066=CARTESIAN_POINT ( 'NONE',  ( -15.80959461918071618, 14.24510877297761446, 11.49999999999999645 ) ) ;
#37070=CARTESIAN_POINT ( 'NONE',  ( 18.11909884760711975, -12.84011383348296853, -1.500000000000002220 ) ) ;
#37071=EDGE_CURVE ( 'NONE', #60342, #31523, #49855, .T. ) ;
#37072=CARTESIAN_POINT ( 'NONE',  ( -0.003042231299257275486, -20.61035990087709635, -1.500000000000002220 ) ) ;
#37073=ORIENTED_EDGE ( 'NONE', *, *, #99459, .F. ) ;
#37076=CARTESIAN_POINT ( 'NONE',  ( -56.62287095715007013, -23.96127896941632685, -0.6493128931037894791 ) ) ;
#37080=CARTESIAN_POINT ( 'NONE',  ( -125.7765849230966211, -25.21250125880508719, 3.500947807641615839 ) ) ;
#37081=CARTESIAN_POINT ( 'NONE',  ( -41.58697324491572545, -24.35071581493542325, 9.817618358456032368 ) ) ;
#37082=CARTESIAN_POINT ( 'NONE',  ( -99.62287095715005592, -29.50248528299804818, 1.056150453629042030 ) ) ;
#37083=CARTESIAN_POINT ( 'NONE',  ( 0.5783248939474509021, 20.82821387695577187, -1.500000000000002220 ) ) ;
#37084=ADVANCED_FACE ( 'NONE', ( #26997 ), #97002, .F. ) ;
#37085=CARTESIAN_POINT ( 'NONE',  ( -16.40380107638378604, 14.33077157581830008, 11.49999999999999645 ) ) ;
#37086=CARTESIAN_POINT ( 'NONE',  ( -51.88024557362344069, -25.20637680390643354, 6.555349849948861163 ) ) ;
#37088=CARTESIAN_POINT ( 'NONE',  ( -8.519796113377745783, 20.75715399588506926, 11.49999999999998934 ) ) ;
#37089=AXIS2_PLACEMENT_3D ( 'NONE', #36957, #91240, #83626 ) ;
#37092=CARTESIAN_POINT ( 'NONE',  ( -71.50913726475666010, -25.30966908743296884, 5.397536596095833694 ) ) ;
#37093=CARTESIAN_POINT ( 'NONE',  ( -66.52287095715006160, -29.50247984919015209, -1.443849546365055359 ) ) ;
#37094=ORIENTED_EDGE ( 'NONE', *, *, #74433, .F. ) ;
#37095=AXIS2_PLACEMENT_3D ( 'NONE', #60029, #5722, #4234 ) ;
#37096=VERTEX_POINT ( 'NONE', #11266 ) ;
#37097=CARTESIAN_POINT ( 'NONE',  ( -99.70017921987172826, -25.30826663797894227, 5.426235228613150774 ) ) ;
#37099=CARTESIAN_POINT ( 'NONE',  ( 1.764508054474889009, 21.21474994468914943, -1.500000000000002220 ) ) ;
#37100=ORIENTED_EDGE ( 'NONE', *, *, #99069, .F. ) ;
#37102=CARTESIAN_POINT ( 'NONE',  ( -0.5131542516139314669, 21.03015271272555253, 11.49999999999998934 ) ) ;
#37103=CARTESIAN_POINT ( 'NONE',  ( -38.52287095715006160, -24.50321055353803956, 9.387540953477520489 ) ) ;
#37105=B_SPLINE_CURVE_WITH_KNOTS ( 'NONE', 3,
 ( #41337, #64195, #85497, #86003, #40827, #25607 ),
 .UNSPECIFIED., .F., .F.,
 ( 4, 2, 4 ),
 ( 0.000000000000000000, 0.001380764517853250986, 0.002761529035706501971 ),
 .UNSPECIFIED. ) ;
#37108=CARTESIAN_POINT ( 'NONE',  ( 5.197331492371871420, 21.31670716312865466, -1.500000000000002220 ) ) ;
#37109=CARTESIAN_POINT ( 'NONE',  ( -87.59165601682460078, -24.15543982623908548, -0.2315651400026449980 ) ) ;
#37111=CARTESIAN_POINT ( 'NONE',  ( -80.71590087609354214, -25.30702814991555982, 4.545935848987151751 ) ) ;
#37112=EDGE_CURVE ( 'NONE', #57878, #89671, #53318, .T. ) ;
#37114=CARTESIAN_POINT ( 'NONE',  ( -84.62619856286293896, -24.51419770103157347, 9.386484678747175181 ) ) ;
#37115=CARTESIAN_POINT ( 'NONE',  ( -130.5728709571500588, -24.66459861931856778, 1.095224832288515637 ) ) ;
#37116=CARTESIAN_POINT ( 'NONE',  ( -30.62895736903226407, -24.04695220404052591, 10.47594215909544779 ) ) ;
#37117=CARTESIAN_POINT ( 'NONE',  ( 20.49606604269246546, -5.804284187783010474, -1.500000000000002220 ) ) ;
#37118=CARTESIAN_POINT ( 'NONE',  ( -98.54622777176759030, -24.66019654487200086, 8.947790411086115725 ) ) ;
#37120=ADVANCED_FACE ( 'NONE', ( #81778 ), #98557, .T. ) ;
#37121=DIRECTION ( 'NONE',  ( -3.773278334453079030E-23, 0.9999999999976377785, 2.173523156925979128E-06 ) ) ;
#37122=CARTESIAN_POINT ( 'NONE',  ( -70.52287095715007581, -24.62226745350440282, 0.9660975649729651726 ) ) ;
#37123=CARTESIAN_POINT ( 'NONE',  ( 20.43785579724129420, 9.289222182981756504, -1.500000000000002220 ) ) ;
#37125=EDGE_CURVE ( 'NONE', #39121, #77364, #81173, .T. ) ;
#37126=CARTESIAN_POINT ( 'NONE',  ( -110.9410897254133204, -25.11552134530501590, 2.805129186380271644 ) ) ;
#37127=VERTEX_POINT ( 'NONE', #37600 ) ;
#37128=CARTESIAN_POINT ( 'NONE',  ( -81.52287095715006160, -23.48786465467241058, 11.44779295918254469 ) ) ;
#37129=CARTESIAN_POINT ( 'NONE',  ( 19.59260286812380514, -1.442238090573773501, 11.49999999999999645 ) ) ;
#37130=CARTESIAN_POINT ( 'NONE',  ( -66.62287095715007013, -24.51387760970723662, 9.387446482453425389 ) ) ;
#37131=CARTESIAN_POINT ( 'NONE',  ( -63.52287095715006160, -23.47596703998600631, 11.44779298504228926 ) ) ;
#37133=LINE ( 'NONE', #59989, #19827 ) ;
#37134=CARTESIAN_POINT ( 'NONE',  ( -100.6228709571500559, -23.47593901973091235, -1.443836447539001089 ) ) ;
#37135=CARTESIAN_POINT ( 'NONE',  ( -99.85057463794808541, -25.25095808762917571, 5.344630504190060805 ) ) ;
#37136=CARTESIAN_POINT ( 'NONE',  ( -62.62287095715004881, -23.47596703998600276, 11.44779298504227505 ) ) ;
#37137=CARTESIAN_POINT ( 'NONE',  ( -2.355416116969162754, -19.56741566493107598, -1.500000000000002220 ) ) ;
#37138=B_SPLINE_CURVE_WITH_KNOTS ( 'NONE', 3,
 ( #89472, #5229, #35687, #36185 ),
 .UNSPECIFIED., .F., .F.,
 ( 4, 4 ),
 ( 0.000000000000000000, 0.0001000000000000028644 ),
 .UNSPECIFIED. ) ;
#37139=VERTEX_POINT ( 'NONE', #90389 ) ;
#37141=B_SPLINE_CURVE_WITH_KNOTS ( 'NONE', 3,
 ( #46892, #9822, #55510, #78320, #71733, #93046 ),
 .UNSPECIFIED., .F., .F.,
 ( 4, 2, 4 ),
 ( 1.570887131794176733E-05, 0.001396322306279759555, 0.002776935741241577573 ),
 .UNSPECIFIED. ) ;
#37145=ORIENTED_EDGE ( 'NONE', *, *, #38540, .T. ) ;
#37146=DIRECTION ( 'NONE',  ( -0.000000000000000000, 2.173523156925979552E-06, -0.9999999999976378895 ) ) ;
#37148=CARTESIAN_POINT ( 'NONE',  ( -90.58953762381672448, -23.48786465467241058, 11.44779295918254469 ) ) ;
#37149=PLANE ( 'NONE',  #93084 ) ;
#37151=ADVANCED_FACE ( 'NONE', ( #99484 ), #24251, .F. ) ;
#37154=CARTESIAN_POINT ( 'NONE',  ( -122.5228709571500616, -29.50250786944525672, 11.44777988621622811 ) ) ;
#37155=CARTESIAN_POINT ( 'NONE',  ( -19.59816365915598979, -3.832847594873297403, -1.500000000000002220 ) ) ;
#37157=CARTESIAN_POINT ( 'NONE',  ( -51.69889270095674760, -25.27742702178395717, 4.038250842609248714 ) ) ;
#37158=ORIENTED_EDGE ( 'NONE', *, *, #55074, .F. ) ;
#37162=ADVANCED_FACE ( 'NONE', ( #75645 ), #44225, .T. ) ;
#37163=B_SPLINE_CURVE_WITH_KNOTS ( 'NONE', 3,
 ( #6616, #46693, #8124, #70014, #39064, #501 ),
 .UNSPECIFIED., .F., .F.,
 ( 4, 2, 4 ),
 ( 0.000000000000000000, 0.001380901958385397869, 0.002761803916770795737 ),
 .UNSPECIFIED. ) ;
#37165=CARTESIAN_POINT ( 'NONE',  ( -119.5910507080879199, -23.96119346886881019, -0.6495511937832016969 ) ) ;
#37166=FACE_OUTER_BOUND ( 'NONE', #50184, .T. ) ;
#37168=CARTESIAN_POINT ( 'NONE',  ( -39.65632424235193554, -23.73766607897669800, -1.055555164236461341 ) ) ;
#37169=VECTOR ( 'NONE', #61019, 1000.000000000000114 ) ;
#37173=CARTESIAN_POINT ( 'NONE',  ( -34.62287095715004170, -23.73907113216990439, -1.053371485793236806 ) ) ;
#37174=LINE ( 'NONE', #43302, #50087 ) ;
#37176=CARTESIAN_POINT ( 'NONE',  ( -19.75413285895528404, 4.560271753130525241, 11.49999999999998934 ) ) ;
#37178=CARTESIAN_POINT ( 'NONE',  ( -39.62287095715005592, -24.64898659630366851, 1.056161002820819261 ) ) ;
#37180=CARTESIAN_POINT ( 'NONE',  ( -76.62287095715007013, -24.34917612406837861, 0.1852690917426645656 ) ) ;
#37183=CARTESIAN_POINT ( 'NONE',  ( -82.62287095715005592, -29.50250243563736774, 8.947779886222141599 ) ) ;
#37184=CARTESIAN_POINT ( 'NONE',  ( -7.184633862932894743, 18.80532529184710100, -1.500000000000002220 ) ) ;
#37185=CARTESIAN_POINT ( 'NONE',  ( -2.902382693073098707, -20.91247731031871382, 11.49999999999999645 ) ) ;
#37186=CARTESIAN_POINT ( 'NONE',  ( -94.62287095715005592, -29.50248528299804818, 1.056150453629040253 ) ) ;
#37187=CARTESIAN_POINT ( 'NONE',  ( 14.53198226072946220, 16.64418356588832992, 11.49999999999998934 ) ) ;
#37189=CARTESIAN_POINT ( 'NONE',  ( 16.23509277041898358, 12.58620111108425377, -1.500000000000002220 ) ) ;
#37190=CARTESIAN_POINT ( 'NONE',  ( -39.44984910185593208, -25.27805931940480377, 4.278338840711595203 ) ) ;
#37195=ORIENTED_EDGE ( 'NONE', *, *, #45043, .T. ) ;
#37196=ADVANCED_FACE ( 'NONE', ( #83764 ), #14247, .F. ) ;
#37197=CARTESIAN_POINT ( 'NONE',  ( -99.13315347086529528, -25.26009968875505507, 3.839156536065280623 ) ) ;
#37198=B_SPLINE_SURFACE_WITH_KNOTS ( 'NONE', 3, 3, ( 
 ( #7815, #53515, #38260, #38758 ),
 ( #84438, #69218, #69727, #205 ),
 ( #8821, #45891, #29655, #68228 ),
 ( #99157, #91551, #31150, #100133 ),
 ( #70221, #54497, #22024, #62119 ),
 ( #93041, #85432, #76314, #6813 ),
 ( #37771, #18430, #40271, #1214 ) ),
 .UNSPECIFIED., .F., .F., .F.,
 ( 4, 3, 4 ),
 ( 4, 4 ),
 ( 0.0004766839783819933041, 0.1029713700210895672, 0.2054660560637971423 ),
 ( 0.3695880141246808970, 0.3707712659113398534 ),
 .UNSPECIFIED. ) ;
#37199=CARTESIAN_POINT ( 'NONE',  ( -102.5895376238167245, -23.47596703998600631, 11.44779298504227683 ) ) ;
#37201=EDGE_LOOP ( 'NONE', ( #12524, #9863, #36627, #86731 ) ) ;
#37204=CARTESIAN_POINT ( 'NONE',  ( -76.50807368432518274, -24.15543982623907482, -0.2315651400026599582 ) ) ;
#37205=CARTESIAN_POINT ( 'NONE',  ( 3.086129920417311823, 20.35385046113321295, -1.500000000000002220 ) ) ;
#37206=EDGE_CURVE ( 'NONE', #4570, #51553, #32634, .T. ) ;
#37207=CARTESIAN_POINT ( 'NONE',  ( 5.568959250215116619, -20.88136358707659923, 11.49999999999999645 ) ) ;
#37208=ORIENTED_EDGE ( 'NONE', *, *, #83143, .F. ) ;
#37211=CARTESIAN_POINT ( 'NONE',  ( -5.491053050139323766, 21.65304554001118120, -1.500000000000002220 ) ) ;
#37215=VERTEX_POINT ( 'NONE', #64855 ) ;
#37216=ADVANCED_FACE ( 'NONE', ( #63847 ), #39978, .T. ) ;
#37218=CARTESIAN_POINT ( 'NONE',  ( -35.52468542394368001, -24.83644354573578639, 8.397322867130093016 ) ) ;
#37219=CARTESIAN_POINT ( 'NONE',  ( 12.60132613692001691, 16.66296579206088069, -1.500000000000002220 ) ) ;
#37220=ORIENTED_EDGE ( 'NONE', *, *, #49978, .T. ) ;
#37221=CARTESIAN_POINT ( 'NONE',  ( -67.53677154461657040, -24.66019654487199730, 8.947790411086115725 ) ) ;
#37224=B_SPLINE_CURVE_WITH_KNOTS ( 'NONE', 3,
 ( #40711, #57457, #66579, #65080 ),
 .UNSPECIFIED., .F., .F.,
 ( 4, 4 ),
 ( 0.6202288146924654910, 0.6292352459645811358 ),
 .UNSPECIFIED. ) ;
#37225=DIRECTION ( 'NONE',  ( -3.773278334453079030E-23, 0.9999999999976377785, 2.173523156925979128E-06 ) ) ;
#37226=CARTESIAN_POINT ( 'NONE',  ( -4.502559807402421121, -20.62786074129878955, -1.500000000000002220 ) ) ;
#37227=ORIENTED_EDGE ( 'NONE', *, *, #65268, .F. ) ;
#37228=CARTESIAN_POINT ( 'NONE',  ( -117.5209660606645627, -23.73766607897671221, -1.055555164236445576 ) ) ;
#37229=CARTESIAN_POINT ( 'NONE',  ( -100.4426124108961176, -25.12215675263029624, 7.101635560846706774 ) ) ;
#37230=CARTESIAN_POINT ( 'NONE',  ( -21.05831370385527990, 5.553659732266172711, 11.49999999999998934 ) ) ;
#37234=CARTESIAN_POINT ( 'NONE',  ( -79.34687923781922336, -25.27781941911278807, 5.960409260969139922 ) ) ;
#37235=CARTESIAN_POINT ( 'NONE',  ( 16.02445091669267185, 14.69945503153335764, -1.500000000000002220 ) ) ;
#37236=CARTESIAN_POINT ( 'NONE',  ( -71.20541289166536103, -25.31639469619771177, 4.885889946353112023 ) ) ;
#37237=CARTESIAN_POINT ( 'NONE',  ( 20.12748746789148413, 9.599020362109589755, 11.49999999999999645 ) ) ;
#37238=VERTEX_POINT ( 'NONE', #94760 ) ;
#37239=CARTESIAN_POINT ( 'NONE',  ( -57.52287095715004028, -24.51387760970724372, 9.387446482453414731 ) ) ;
#37240=CARTESIAN_POINT ( 'NONE',  ( -70.52287095715007581, -23.47596703998600631, 11.44779298504228748 ) ) ;
#37241=PLANE ( 'NONE',  #13199 ) ;
#37244=ORIENTED_EDGE ( 'NONE', *, *, #24448, .T. ) ;
#37246=ORIENTED_EDGE ( 'NONE', *, *, #17913, .F. ) ;
#37249=CARTESIAN_POINT ( 'NONE',  ( 21.17954554857512761, 0.9134790845329443520, -1.500000000000002220 ) ) ;
#37251=CARTESIAN_POINT ( 'NONE',  ( -80.51244414166535535, -25.27791972951919774, 7.563173683831821315 ) ) ;
#37253=B_SPLINE_CURVE_WITH_KNOTS ( 'NONE', 3,
 ( #19980, #91481, #97604, #5257 ),
 .UNSPECIFIED., .F., .F.,
 ( 4, 4 ),
 ( 0.000000000000000000, 9.999999999996816991E-05 ),
 .UNSPECIFIED. ) ;
#37256=CARTESIAN_POINT ( 'NONE',  ( -16.26263985875334228, -10.51264992557365829, 11.49999999999998934 ) ) ;
#37257=CARTESIAN_POINT ( 'NONE',  ( -38.52287095715008292, -23.72747288104469732, -1.053458166803227680 ) ) ;
#37258=ORIENTED_EDGE ( 'NONE', *, *, #62915, .F. ) ;
#37259=CARTESIAN_POINT ( 'NONE',  ( -15.63568348323273227, -11.59263941501104966, 11.49999999999999645 ) ) ;
#37260=CARTESIAN_POINT ( 'NONE',  ( -115.5228709571500190, -24.63345952396256067, 9.038047939301504741 ) ) ;
#37261=ORIENTED_EDGE ( 'NONE', *, *, #73888, .F. ) ;
#37264=LINE ( 'NONE', #28156, #74104 ) ;
#37265=FACE_OUTER_BOUND ( 'NONE', #6752, .T. ) ;
#37266=CARTESIAN_POINT ( 'NONE',  ( -10.75157073690095721, 16.42123490324765811, -1.500000000000002220 ) ) ;
#37267=LINE ( 'NONE', #68218, #44486 ) ;
#37268=ORIENTED_EDGE ( 'NONE', *, *, #75741, .T. ) ;
#37269=CARTESIAN_POINT ( 'NONE',  ( 21.29926025483437257, -3.289820829717503337, 11.49999999999998934 ) ) ;
#37270=CARTESIAN_POINT ( 'NONE',  ( -33.63538797308950734, -24.35071581493542325, 9.817618358456039473 ) ) ;
#37272=CARTESIAN_POINT ( 'NONE',  ( -115.5228709571500616, -24.99132157543084531, 2.256160258750667502 ) ) ;
#37274=CARTESIAN_POINT ( 'NONE',  ( 0.1381291366035634904, -23.06709338131901532, -1.500000000000002220 ) ) ;
#37277=CARTESIAN_POINT ( 'NONE',  ( -101.6228709571500559, -29.50250786944525672, 11.44777988621623166 ) ) ;
#37278=CARTESIAN_POINT ( 'NONE',  ( -50.10132759428470450, -25.25249061358302782, 3.767456410489268936 ) ) ;
#37279=CARTESIAN_POINT ( 'NONE',  ( -8.609638109768802394, 18.19638482192696216, 11.49999999999999645 ) ) ;
#37280=CARTESIAN_POINT ( 'NONE',  ( -84.62287095715007013, -24.50321055353803601, 9.387540953477522265 ) ) ;
#37284=CARTESIAN_POINT ( 'NONE',  ( -63.62287095715004881, -29.50250243563736774, 8.947779886222145151 ) ) ;
#37285=CARTESIAN_POINT ( 'NONE',  ( 11.60740158406642664, -16.16820694497113564, -1.500000000000002220 ) ) ;
#37286=CARTESIAN_POINT ( 'NONE',  ( -69.22287095715007865, -23.47593901973090169, -1.443836447538997536 ) ) ;
#37287=ADVANCED_FACE ( 'NONE', ( #9529 ), #18632, .T. ) ;
#37288=CARTESIAN_POINT ( 'NONE',  ( -17.60924879254659459, 8.996216891746938060, -1.500000000000002220 ) ) ;
#37290=CARTESIAN_POINT ( 'NONE',  ( -42.62371182274537773, -24.65952944569304606, 1.056160979905694353 ) ) ;
#37291=SHAPE_REPRESENTATION ( 'Measuring Tape_Varsay\X2\0131\X0\lan', ( #218 ), #69909 ) ;
#37292=EDGE_CURVE ( 'NONE', #1762, #70610, #31555, .T. ) ;
#37293=B_SPLINE_CURVE_WITH_KNOTS ( 'NONE', 3,
 ( #37778, #74834, #68733, #44907 ),
 .UNSPECIFIED., .F., .F.,
 ( 4, 4 ),
 ( 0.9912077972255933789, 0.9999675692521627912 ),
 .UNSPECIFIED. ) ;
#37297=CARTESIAN_POINT ( 'NONE',  ( -16.33875328525262560, 12.67428768300982256, 11.49999999999999645 ) ) ;
#37298=CARTESIAN_POINT ( 'NONE',  ( -66.62287095715005592, -23.47593901973091235, -1.443836447539006196 ) ) ;
#37300=CARTESIAN_POINT ( 'NONE',  ( -97.62287095715005592, -24.64965695001468404, 8.947790433994178727 ) ) ;
#37301=DIRECTION ( 'NONE',  ( 0.000000000000000000, -0.9999999999976377785, -2.173523156925979128E-06 ) ) ;
#37302=CARTESIAN_POINT ( 'NONE',  ( -9.076218414377828836, -20.82814578352222767, 11.49999999999999645 ) ) ;
#37303=EDGE_LOOP ( 'NONE', ( #30524, #96117, #5681, #9803 ) ) ;
#37304=CARTESIAN_POINT ( 'NONE',  ( -46.62287095715003460, -23.73934037231756733, 11.05740245334329153 ) ) ;
#37307=CARTESIAN_POINT ( 'NONE',  ( 3.569899647507075890, 19.86734082857295647, -1.500000000000002220 ) ) ;
#37310=CARTESIAN_POINT ( 'NONE',  ( -41.46611000704998418, -25.27828342519987359, 4.188173683033348915 ) ) ;
#37312=VERTEX_POINT ( 'NONE', #49114 ) ;
#37313=EDGE_CURVE ( 'NONE', #25230, #28727, #40017, .T. ) ;
#37315=CARTESIAN_POINT ( 'NONE',  ( -19.55383134093860420, 11.88776249338449986, -1.500000000000002220 ) ) ;
#37316=DIRECTION ( 'NONE',  ( -0.000000000000000000, 2.173523156925979552E-06, -0.9999999999976378895 ) ) ;
#37317=AXIS2_PLACEMENT_3D ( 'NONE', #12510, #98234, #21111 ) ;
#37318=CARTESIAN_POINT ( 'NONE',  ( -19.46174652491427182, -9.421329337880418819, -1.500000000000002220 ) ) ;
#37319=CARTESIAN_POINT ( 'NONE',  ( -123.6238847173920732, -24.51314013834316796, 0.6176544820404235026 ) ) ;
#37320=CARTESIAN_POINT ( 'NONE',  ( -34.48367125095467145, -24.51314013834315375, 0.6176544820404091807 ) ) ;
#37321=CARTESIAN_POINT ( 'NONE',  ( -17.14161228048114438, 11.91956482804130601, 11.49999999999999645 ) ) ;
#37324=DIRECTION ( 'NONE',  ( 0.000000000000000000, -0.9999999999976377785, -2.173523156925979975E-06 ) ) ;
#37325=CARTESIAN_POINT ( 'NONE',  ( -4.682628417673765142, 21.48327871026360114, -1.500000000000002220 ) ) ;
#37328=CARTESIAN_POINT ( 'NONE',  ( -105.5543609335628901, -24.15602025860896163, 10.28564288303535967 ) ) ;
#37329=CARTESIAN_POINT ( 'NONE',  ( -40.81364289383298427, -25.29087043510296340, 2.874305797121810446 ) ) ;
#37330=ORIENTED_EDGE ( 'NONE', *, *, #53893, .F. ) ;
#37331=CARTESIAN_POINT ( 'NONE',  ( -25.53098197642538736, -24.91566218739149363, 4.942811707542018596 ) ) ;
#37332=CARTESIAN_POINT ( 'NONE',  ( -90.62618068010999650, -24.83644354573578994, 8.397322867130100121 ) ) ;
#37333=ORIENTED_EDGE ( 'NONE', *, *, #6213, .T. ) ;
#37334=CARTESIAN_POINT ( 'NONE',  ( -72.58793278032496232, -24.35071581493543036, 9.817618358456032368 ) ) ;
#37335=ORIENTED_EDGE ( 'NONE', *, *, #24334, .T. ) ;
#37336=B_SPLINE_CURVE_WITH_KNOTS ( 'NONE', 3,
 ( #18216, #80111, #33436, #41059 ),
 .UNSPECIFIED., .F., .F.,
 ( 4, 4 ),
 ( 0.000000000000000000, 9.999999999997510880E-05 ),
 .UNSPECIFIED. ) ;
#37337=VERTEX_POINT ( 'NONE', #95765 ) ;
#37338=CARTESIAN_POINT ( 'NONE',  ( -71.62697017891946416, -24.51419770103159124, 9.386484678747166299 ) ) ;
#37339=CARTESIAN_POINT ( 'NONE',  ( -106.6228709571500559, -29.50247984919015209, -1.443849546365048253 ) ) ;
#37340=CARTESIAN_POINT ( 'NONE',  ( -103.2228709571500787, -23.47593901973090169, -1.443836447538996648 ) ) ;
#37341=CARTESIAN_POINT ( 'NONE',  ( -20.33632446988539400, 1.880062042347348195, -1.500000000000002220 ) ) ;
#37342=EDGE_CURVE ( 'NONE', #79371, #20842, #17139, .T. ) ;
#37345=CARTESIAN_POINT ( 'NONE',  ( -30.60464735295150263, -24.58764167366260622, 9.439037205594624780 ) ) ;
#37346=EDGE_CURVE ( 'NONE', #84649, #33464, #72442, .T. ) ;
#37347=CARTESIAN_POINT ( 'NONE',  ( -80.13654269935770458, -25.20074414427590170, 3.409327697718777195 ) ) ;
#37348=DIRECTION ( 'NONE',  ( 0.000000000000000000, -0.9999999999976377785, -2.173523156925979128E-06 ) ) ;
#37350=B_SPLINE_CURVE_WITH_KNOTS ( 'NONE', 3,
 ( #51151, #18690, #73003, #96821 ),
 .UNSPECIFIED., .F., .F.,
 ( 4, 4 ),
 ( 0.3289991091667107126, 0.3299998562074764052 ),
 .UNSPECIFIED. ) ;
#37351=FACE_OUTER_BOUND ( 'NONE', #18837, .T. ) ;
#37352=CARTESIAN_POINT ( 'NONE',  ( -29.81002072791678614, -25.26247421725459930, 5.237831151396452611 ) ) ;
#37353=CARTESIAN_POINT ( 'NONE',  ( 15.20108283357335921, -14.20388156210760577, 11.49999999999998934 ) ) ;
#37354=B_SPLINE_CURVE_WITH_KNOTS ( 'NONE', 3,
 ( #13787, #83808, #51876, #66622 ),
 .UNSPECIFIED., .F., .F.,
 ( 4, 4 ),
 ( 0.000000000000000000, 1.000000000000000000 ),
 .UNSPECIFIED. ) ;
#37355=ORIENTED_EDGE ( 'NONE', *, *, #89778, .T. ) ;
#37356=LINE ( 'NONE', #14496, #68144 ) ;
#37359=ORIENTED_EDGE ( 'NONE', *, *, #35012, .F. ) ;
#37362=CARTESIAN_POINT ( 'NONE',  ( -128.6228709571500417, -24.64898659630529565, 1.056161002820834804 ) ) ;
#37363=CARTESIAN_POINT ( 'NONE',  ( -118.8949125657484274, -25.24693556693654273, 3.801660433955579954 ) ) ;
#37364=CARTESIAN_POINT ( 'NONE',  ( -40.62287095715005592, -24.83620972994591725, 8.398175272781363887 ) ) ;
#37365=CARTESIAN_POINT ( 'NONE',  ( -92.62813586326385007, -24.35071581493543391, 9.817618358456025263 ) ) ;
#37366=CARTESIAN_POINT ( 'NONE',  ( -100.5562042904833930, -25.00182538069145366, 7.747789668545099317 ) ) ;
#37367=CARTESIAN_POINT ( 'NONE',  ( 21.88104185797606505, 3.448541436957560880, 11.49999999999999645 ) ) ;
#37368=ORIENTED_EDGE ( 'NONE', *, *, #80963, .F. ) ;
#37369=CARTESIAN_POINT ( 'NONE',  ( -108.5864066755810029, -24.65952944569305316, 1.056160979905706121 ) ) ;
#37370=CARTESIAN_POINT ( 'NONE',  ( -22.62345309801473547, -0.4825844212548152656, 11.49999999999998934 ) ) ;
#37371=CARTESIAN_POINT ( 'NONE',  ( -111.5228709571500332, -24.51387760970725083, 9.387446482453398744 ) ) ;
#37373=VERTEX_POINT ( 'NONE', #57231 ) ;
#37374=CARTESIAN_POINT ( 'NONE',  ( -81.26427307513701237, -25.31500402857158605, 5.136443472453636083 ) ) ;
#37376=CARTESIAN_POINT ( 'NONE',  ( 0.3675393366473880818, 20.13074986235200470, -1.500000000000002220 ) ) ;
#37377=CARTESIAN_POINT ( 'NONE',  ( -65.62287095715005592, -23.47593901973091235, -1.443836447539006196 ) ) ;
#37379=CARTESIAN_POINT ( 'NONE',  ( -53.62287095715005592, -23.47593901973091235, -1.443836447539009749 ) ) ;
#37380=CARTESIAN_POINT ( 'NONE',  ( -2.938769918389303459, -22.12206158279486345, -1.500000000000002220 ) ) ;
#37381=EDGE_LOOP ( 'NONE', ( #1867, #29977, #73328, #72496 ) ) ;
#37383=CARTESIAN_POINT ( 'NONE',  ( -101.3987937098823409, -25.16257383815580440, 6.605699142167675397 ) ) ;
#37385=DIRECTION ( 'NONE',  ( -3.773278334444166432E-23, 1.000000000000000000, 0.000000000000000000 ) ) ;
#37387=FACE_OUTER_BOUND ( 'NONE', #37876, .T. ) ;
#37389=CARTESIAN_POINT ( 'NONE',  ( -4.042178566331402045, 19.10766070095605684, 11.49999999999998934 ) ) ;
#37390=PLANE ( 'NONE',  #57137 ) ;
#37392=CARTESIAN_POINT ( 'NONE',  ( -8.943896628894790979, 19.53434260886740503, 11.49999999999998934 ) ) ;
#37395=CARTESIAN_POINT ( 'NONE',  ( -120.5228709571500616, -24.99156044556120904, 7.747789690856173195 ) ) ;
#37396=CARTESIAN_POINT ( 'NONE',  ( -17.76840699843883442, -14.40508365592194195, -1.500000000000002220 ) ) ;
#37399=CARTESIAN_POINT ( 'NONE',  ( -106.5908009524538471, -24.15620529776629510, 10.23563542870659582 ) ) ;
#37400=CARTESIAN_POINT ( 'NONE',  ( -127.5228709571500616, -23.47593901973090524, -1.443836447538996204 ) ) ;
#37401=CARTESIAN_POINT ( 'NONE',  ( -14.87316555497233495, -13.31901947624662519, 11.49999999999999645 ) ) ;
#37402=FACE_OUTER_BOUND ( 'NONE', #84241, .T. ) ;
#37403=EDGE_CURVE ( 'NONE', #11321, #55957, #66838, .T. ) ;
#37404=EDGE_CURVE ( 'NONE', #6142, #56961, #25450, .T. ) ;
#37405=CARTESIAN_POINT ( 'NONE',  ( -74.54988272486899348, -24.15620529776628800, 10.23563542870659937 ) ) ;
#37408=CARTESIAN_POINT ( 'NONE',  ( -48.62287095715004881, -29.50248528299804818, 1.056150453629033370 ) ) ;
#37410=ADVANCED_FACE ( 'NONE', ( #52093 ), #36866, .F. ) ;
#37411=CARTESIAN_POINT ( 'NONE',  ( 18.95625057990686813, 10.65820999021175730, -1.500000000000002220 ) ) ;
#37413=CARTESIAN_POINT ( 'NONE',  ( -15.21066300689680872, 12.40131300380995860, -1.500000000000002220 ) ) ;
#37414=EDGE_CURVE ( 'NONE', #45193, #1888, #12150, .T. ) ;
#37415=CARTESIAN_POINT ( 'NONE',  ( -34.52287095715006160, -23.96127896942118696, -0.6493128930941864940 ) ) ;
#37416=ORIENTED_EDGE ( 'NONE', *, *, #39916, .T. ) ;
#37418=PLANE ( 'NONE',  #85620 ) ;
#37420=CARTESIAN_POINT ( 'NONE',  ( 20.49162120248849561, -0.4999214236376636200, 11.49999999999999645 ) ) ;
#37424=CARTESIAN_POINT ( 'NONE',  ( -109.3610823860251031, -25.28402660629545196, 4.275462642134054470 ) ) ;
#37425=CARTESIAN_POINT ( 'NONE',  ( -40.45829750704998418, -25.28892422092284065, 3.293942890672450829 ) ) ;
#37426=CARTESIAN_POINT ( 'NONE',  ( -116.5208648445381243, -23.73791477778912551, 11.05961554403170055 ) ) ;
#37427=CARTESIAN_POINT ( 'NONE',  ( -85.52287095715004739, -25.00158670708909625, 2.256160236439166411 ) ) ;
#37428=CARTESIAN_POINT ( 'NONE',  ( -124.6228709571500559, -23.48786465467241769, 11.44779295918253759 ) ) ;
#37430=CARTESIAN_POINT ( 'NONE',  ( -0.07435467474217070938, 23.09247799282200475, 11.49999999999999645 ) ) ;
#37431=CARTESIAN_POINT ( 'NONE',  ( 15.15630024635751383, 17.02982414992789018, -1.500000000000002220 ) ) ;
#37432=CARTESIAN_POINT ( 'NONE',  ( -110.6281927241458476, -24.40133493613049964, 9.663955038902800609 ) ) ;
#37436=CARTESIAN_POINT ( 'NONE',  ( -110.5527842940492889, -24.40034930558991633, 0.3402023900116072364 ) ) ;
#37437=VECTOR ( 'NONE', #30255, 1000.000000000000114 ) ;
#37438=CARTESIAN_POINT ( 'NONE',  ( 11.09338859787202480, -18.89396691112096605, -1.500000000000002220 ) ) ;
#37439=CARTESIAN_POINT ( 'NONE',  ( -129.6228709571500417, -24.66019654487200086, 8.947790411086117501 ) ) ;
#37441=CARTESIAN_POINT ( 'NONE',  ( -77.62287095715005592, -23.73907113216990794, -1.053371485793230145 ) ) ;
#37442=CARTESIAN_POINT ( 'NONE',  ( -78.62656218994159474, -24.51314013834315375, 0.6176544820404143987 ) ) ;
#37443=CARTESIAN_POINT ( 'NONE',  ( -94.62287095715001328, -23.96177878511308634, 10.65340807706329507 ) ) ;
#37444=CARTESIAN_POINT ( 'NONE',  ( -107.6228709571500701, -24.50321055353805377, 9.387540953477529371 ) ) ;
#37445=EDGE_LOOP ( 'NONE', ( #10870, #5959, #10886, #84812 ) ) ;
#37446=CARTESIAN_POINT ( 'NONE',  ( 13.31029742451639386, -15.53102932315203510, 11.49999999999998934 ) ) ;
#37447=ORIENTED_EDGE ( 'NONE', *, *, #21145, .T. ) ;
#37450=VERTEX_POINT ( 'NONE', #43492 ) ;
#37451=CARTESIAN_POINT ( 'NONE',  ( 19.24196208499951055, 12.69117723712289703, -1.500000000000002220 ) ) ;
#37452=CARTESIAN_POINT ( 'NONE',  ( -61.63195469153195916, -24.34968618360933945, 0.1864209137778810865 ) ) ;
#37453=CARTESIAN_POINT ( 'NONE',  ( 2.532258636284850706, -20.04889675553949147, -1.500000000000002220 ) ) ;
#37455=CARTESIAN_POINT ( 'NONE',  ( -26.08243833712738180, -24.84481096472645234, 3.118813907533751983 ) ) ;
#37457=ADVANCED_FACE ( 'NONE', ( #74428 ), #26326, .T. ) ;
#37458=B_SPLINE_CURVE_WITH_KNOTS ( 'NONE', 3,
 ( #46652, #69973, #8582, #55268, #100397, #25297 ),
 .UNSPECIFIED., .F., .F.,
 ( 4, 2, 4 ),
 ( 0.000000000000000000, 0.001380901958385382256, 0.002761803916770764512 ),
 .UNSPECIFIED. ) ;
#37460=DIRECTION ( 'NONE',  ( 1.000000000000000000, 3.773278334444167608E-23, 8.201307833595939069E-29 ) ) ;
#37461=LINE ( 'NONE', #23213, #4316 ) ;
#37462=CARTESIAN_POINT ( 'NONE',  ( -16.30254408640404051, -13.89340296626662230, 11.49999999999999645 ) ) ;
#37465=CARTESIAN_POINT ( 'NONE',  ( -61.53494130710347321, -24.66019654487199375, 8.947790411086119278 ) ) ;
#37466=VERTEX_POINT ( 'NONE', #69811 ) ;
#37467=CARTESIAN_POINT ( 'NONE',  ( -19.90621922972506397, 5.769413876575915978, 11.49999999999998934 ) ) ;
#37469=CARTESIAN_POINT ( 'NONE',  ( -71.20541289166536103, -25.31502801509702749, 4.885889949323629189 ) ) ;
#37470=EDGE_LOOP ( 'NONE', ( #75877, #12376, #58925, #45428 ) ) ;
#37471=CARTESIAN_POINT ( 'NONE',  ( -28.58650821181200286, -24.19308601498208233, 0.1864216068622559508 ) ) ;
#37472=VERTEX_POINT ( 'NONE', #76403 ) ;
#37474=ORIENTED_EDGE ( 'NONE', *, *, #49711, .T. ) ;
#37475=CARTESIAN_POINT ( 'NONE',  ( -1.948345350117603125, -21.87844622001750139, 11.49999999999999645 ) ) ;
#37476=CARTESIAN_POINT ( 'NONE',  ( -37.49780277816692120, -24.15620529776627379, 10.23563542870660825 ) ) ;
#37477=CARTESIAN_POINT ( 'NONE',  ( 11.36372850657041589, -19.49111573544105624, -1.500000000000002220 ) ) ;
#37478=CARTESIAN_POINT ( 'NONE',  ( 4.154569570224219355, 20.57273982587956240, -1.500000000000002220 ) ) ;
#37479=DIRECTION ( 'NONE',  ( 1.000000000000000000, 3.773278334444166432E-23, 8.201307841325785021E-29 ) ) ;
#37482=ORIENTED_EDGE ( 'NONE', *, *, #15234, .T. ) ;
#37484=CARTESIAN_POINT ( 'NONE',  ( -66.50060275550248434, -24.34968618360933235, 0.1864209137778773950 ) ) ;
#37485=CARTESIAN_POINT ( 'NONE',  ( 15.50980990363467882, 14.95361599516425244, -1.500000000000002220 ) ) ;
#37486=B_SPLINE_CURVE_WITH_KNOTS ( 'NONE', 3,
 ( #63381, #24782, #86190, #55760 ),
 .UNSPECIFIED., .F., .F.,
 ( 4, 4 ),
 ( 3.505114892038065263E-09, 0.001051774434365497024 ),
 .UNSPECIFIED. ) ;
#37487=CARTESIAN_POINT ( 'NONE',  ( -86.62287095714999907, -24.51387760970724372, 9.387446482453416507 ) ) ;
#37488=ORIENTED_EDGE ( 'NONE', *, *, #91063, .T. ) ;
#37489=CARTESIAN_POINT ( 'NONE',  ( -16.61111445048470614, -13.04167290785011701, -1.500000000000002220 ) ) ;
#37490=CARTESIAN_POINT ( 'NONE',  ( -52.62287095715007013, -24.50321055353805022, 9.387540953477543582 ) ) ;
#37491=CARTESIAN_POINT ( 'NONE',  ( -64.55379694261088730, -23.96119346886879597, -0.6495511937832134652 ) ) ;
#37492=CARTESIAN_POINT ( 'NONE',  ( -83.58262595889972602, -24.66019654487199375, 8.947790411086124607 ) ) ;
#37493=CARTESIAN_POINT ( 'NONE',  ( -61.52287095715006160, -29.50250243563736774, 8.947779886222145151 ) ) ;
#37494=CARTESIAN_POINT ( 'NONE',  ( -100.4381051993576506, -25.11033443737754212, 2.832404817301930056 ) ) ;
#37495=CARTESIAN_POINT ( 'NONE',  ( 2.577866586777615154, 22.04066829813923789, -1.500000000000002220 ) ) ;
#37497=CARTESIAN_POINT ( 'NONE',  ( -71.58081732933524677, -24.65952944569304961, 1.056160979905700570 ) ) ;
#37501=CARTESIAN_POINT ( 'NONE',  ( -41.84702555354165554, -25.27955840369619622, 4.480638990042419501 ) ) ;
#37503=CARTESIAN_POINT ( 'NONE',  ( -14.69715086760845857, -12.76062437926726290, -1.500000000000002220 ) ) ;
#37504=CARTESIAN_POINT ( 'NONE',  ( 6.831138157384286203, 20.27010762675863731, -1.500000000000002220 ) ) ;
#37505=CARTESIAN_POINT ( 'NONE',  ( -38.52287095715006870, -23.73934037231757088, 11.05740245334329153 ) ) ;
#37506=CARTESIAN_POINT ( 'NONE',  ( -74.62287095715005592, -29.50250243563736774, 8.947779886222143375 ) ) ;
#37508=CARTESIAN_POINT ( 'NONE',  ( -123.5228709571500758, -24.33832256527049154, 0.1851278514138671449 ) ) ;
#37509=CARTESIAN_POINT ( 'NONE',  ( -89.52287095715006160, -23.47593901973090169, -1.443836447538996426 ) ) ;
#37510=CARTESIAN_POINT ( 'NONE',  ( -20.05226876979747530, -10.47825485868949613, -1.500000000000002220 ) ) ;
#37513=CARTESIAN_POINT ( 'NONE',  ( -122.5228709571500332, -23.48783264082477018, -1.443836473390084807 ) ) ;
#37514=CARTESIAN_POINT ( 'NONE',  ( -17.60924879254659459, 8.996216891746938060, 11.49999999999999645 ) ) ;
#37517=B_SPLINE_CURVE_WITH_KNOTS ( 'NONE', 3,
 ( #50262, #97422, #89317, #43150, #96927, #19786, #18796, #59366 ),
 .UNSPECIFIED., .F., .F.,
 ( 4, 2, 2, 4 ),
 ( 6.391158118963017816E-06, 0.002007136338672925718, 0.003007508928949907765, 0.004007881519226890246 ),
 .UNSPECIFIED. ) ;
#37518=DIRECTION ( 'NONE',  ( 0.000000000000000000, -2.173523156925979552E-06, 0.9999999999976378895 ) ) ;
#37521=EDGE_CURVE ( 'NONE', #10751, #64821, #17003, .T. ) ;
#37523=CARTESIAN_POINT ( 'NONE',  ( 15.40532884848888884, -15.22192433072940609, 11.49999999999998934 ) ) ;
#37524=CARTESIAN_POINT ( 'NONE',  ( -26.36181591332271168, -24.87490845783449700, 6.596758700703877487 ) ) ;
#37525=CARTESIAN_POINT ( 'NONE',  ( 19.33761327413411024, 2.027444641817329973, -1.500000000000002220 ) ) ;
#37526=EDGE_CURVE ( 'NONE', #25971, #32461, #67883, .T. ) ;
#37528=CARTESIAN_POINT ( 'NONE',  ( -82.62287095715004170, -23.73934037231757799, 11.05740245334328975 ) ) ;
#37529=CARTESIAN_POINT ( 'NONE',  ( 18.78060722631472501, -6.265068672152646734, 11.49999999999998934 ) ) ;
#37530=AXIS2_PLACEMENT_3D ( 'NONE', #32421, #63393, #1983 ) ;
#37531=EDGE_LOOP ( 'NONE', ( #3898, #83648, #94530, #96734 ) ) ;
#37532=EDGE_CURVE ( 'NONE', #66424, #19969, #79902, .T. ) ;
#37534=CARTESIAN_POINT ( 'NONE',  ( 12.41260344771940360, 16.11316662856288318, 11.49999999999999645 ) ) ;
#37536=EDGE_CURVE ( 'NONE', #99338, #39688, #33906, .T. ) ;
#37538=EDGE_LOOP ( 'NONE', ( #20724, #34558, #95889, #69155 ) ) ;
#37539=CARTESIAN_POINT ( 'NONE',  ( -0.03754507760218557533, -22.56394946599023044, 1.600845668900849672 ) ) ;
#37540=CARTESIAN_POINT ( 'NONE',  ( -95.52287095715001897, -24.62285846331437256, 9.038163153548218531 ) ) ;
#37542=CARTESIAN_POINT ( 'NONE',  ( -47.52287095715007581, -23.47593901973090169, -1.443836447538997092 ) ) ;
#37543=CARTESIAN_POINT ( 'NONE',  ( -50.93834974540679639, -25.13772890204246124, 7.016048202706616443 ) ) ;
#37544=CARTESIAN_POINT ( 'NONE',  ( -10.42242239376218116, -17.14354752861867937, 11.49999999999998934 ) ) ;
#37546=CARTESIAN_POINT ( 'NONE',  ( -32.07722060962682775, -24.86441978397624553, 8.247789967200544581 ) ) ;
#37547=EDGE_LOOP ( 'NONE', ( #6992, #27992, #56561, #96238 ) ) ;
#37548=CARTESIAN_POINT ( 'NONE',  ( -63.95380932530888884, -23.56000036390796737, -1.497999999999530818 ) ) ;
#37549=CARTESIAN_POINT ( 'NONE',  ( 22.67525425759127344, 3.225002893152739247, 11.49999999999999645 ) ) ;
#37550=PLANE ( 'NONE',  #9721 ) ;
#37551=CARTESIAN_POINT ( 'NONE',  ( -28.52287095715005449, -23.79850909263262082, -0.6494981837137335789 ) ) ;
#37552=CARTESIAN_POINT ( 'NONE',  ( -59.62287095715004881, -23.47593901973091235, -1.443836447539007972 ) ) ;
#37554=CARTESIAN_POINT ( 'NONE',  ( -113.6228709571500559, -23.48786465467241769, 11.44779295918254114 ) ) ;
#37557=VERTEX_POINT ( 'NONE', #84029 ) ;
#37558=CARTESIAN_POINT ( 'NONE',  ( -20.32544160278596834, -1.370942541838689799, -1.500000000000002220 ) ) ;
#37559=VERTEX_POINT ( 'NONE', #60716 ) ;
#37560=B_SPLINE_CURVE_WITH_KNOTS ( 'NONE', 3,
 ( #82800, #44257, #75186, #68092 ),
 .UNSPECIFIED., .F., .F.,
 ( 4, 4 ),
 ( 4.163336342344337027E-17, 0.001341346153846206812 ),
 .UNSPECIFIED. ) ;
#37561=EDGE_CURVE ( 'NONE', #2264, #57603, #88355, .T. ) ;
#37562=CARTESIAN_POINT ( 'NONE',  ( -1.334576548209915225, -22.92891363262047832, 11.49999999999998934 ) ) ;
#37564=ORIENTED_EDGE ( 'NONE', *, *, #4902, .F. ) ;
#37565=CARTESIAN_POINT ( 'NONE',  ( -108.6235313111936449, -24.66019654487200441, 8.947790411086108620 ) ) ;
#37566=CARTESIAN_POINT ( 'NONE',  ( -77.62661404843181856, -24.51419770103158768, 9.386484678747166299 ) ) ;
#37567=EDGE_CURVE ( 'NONE', #76180, #6118, #18020, .T. ) ;
#37568=CARTESIAN_POINT ( 'NONE',  ( -96.62287095715002749, -23.72747288104441665, -1.053458166803660889 ) ) ;
#37569=CARTESIAN_POINT ( 'NONE',  ( 10.86157628581156764, 18.25448884030880592, 11.49999999999999645 ) ) ;
#37570=ORIENTED_EDGE ( 'NONE', *, *, #60657, .F. ) ;
#37571=B_SPLINE_CURVE_WITH_KNOTS ( 'NONE', 3,
 ( #99150, #6316, #98150, #29650 ),
 .UNSPECIFIED., .F., .F.,
 ( 4, 4 ),
 ( 0.000000000000000000, 0.0001000000000000167422 ),
 .UNSPECIFIED. ) ;
#37572=ORIENTED_EDGE ( 'NONE', *, *, #96714, .T. ) ;
#37573=CARTESIAN_POINT ( 'NONE',  ( 2.577866586777615154, 22.04066829813923789, 11.49999999999998934 ) ) ;
#37575=CARTESIAN_POINT ( 'NONE',  ( -4.647353109605855792, 20.10343637636090719, 11.49999999999998934 ) ) ;
#37576=ORIENTED_EDGE ( 'NONE', *, *, #82237, .F. ) ;
#37577=ORIENTED_EDGE ( 'NONE', *, *, #90154, .T. ) ;
#37579=EDGE_CURVE ( 'NONE', #35568, #85754, #10915, .T. ) ;
#37580=CARTESIAN_POINT ( 'NONE',  ( -54.92287095715006018, -23.47596703998600631, 11.44779298504227683 ) ) ;
#37582=ORIENTED_EDGE ( 'NONE', *, *, #43418, .T. ) ;
#37583=CARTESIAN_POINT ( 'NONE',  ( -121.5228709571500616, -23.47596703998600631, 11.44779298504227860 ) ) ;
#37585=CARTESIAN_POINT ( 'NONE',  ( -1.025521031027718299, 20.81036885881322362, -1.500000000000002220 ) ) ;
#37586=CARTESIAN_POINT ( 'NONE',  ( -3.204121956075930200, -21.57847171274271858, 11.49999999999999645 ) ) ;
#37587=EDGE_CURVE ( 'NONE', #84975, #70943, #16506, .T. ) ;
#37588=CARTESIAN_POINT ( 'NONE',  ( -40.72474911149932097, -25.31583763591767067, 5.047107887422168204 ) ) ;
#37590=CARTESIAN_POINT ( 'NONE',  ( -78.64224600554152289, -23.73791477778911840, 11.05961554403170588 ) ) ;
#37591=CARTESIAN_POINT ( 'NONE',  ( -1.649324495273077451, -22.40575143947253167, -1.500000000000002220 ) ) ;
#37592=CARTESIAN_POINT ( 'NONE',  ( -51.14398700470657388, -25.31296689817077805, 4.389973502500959412 ) ) ;
#37598=ORIENTED_EDGE ( 'NONE', *, *, #65023, .F. ) ;
#37600=CARTESIAN_POINT ( 'NONE',  ( -92.62287095715005592, -24.66019654487199730, 8.947790411086124607 ) ) ;
#37603=CARTESIAN_POINT ( 'NONE',  ( -21.20786952941880443, -2.223526401999901925, -1.500000000000002220 ) ) ;
#37605=CARTESIAN_POINT ( 'NONE',  ( -50.62287095715005592, -25.00182538069145011, 7.747789668545097541 ) ) ;
#37606=CARTESIAN_POINT ( 'NONE',  ( -14.15979099334852798, -15.53166555317341135, 11.49999999999998934 ) ) ;
#37607=CARTESIAN_POINT ( 'NONE',  ( -30.49975201380029333, -24.26950064823562059, 0.04395666736089841320 ) ) ;
#37609=CARTESIAN_POINT ( 'NONE',  ( -64.52287095715006160, -29.50247984919015209, -1.443849546365056913 ) ) ;
#37610=CARTESIAN_POINT ( 'NONE',  ( 0.1985894851802381678, 21.93841921393417849, -1.500000000000002220 ) ) ;
#37611=CARTESIAN_POINT ( 'NONE',  ( -87.52215351861700299, -23.48783264082478794, -1.443836473390063935 ) ) ;
#37612=EDGE_LOOP ( 'NONE', ( #52290, #66589, #39041, #43494 ) ) ;
#37614=CARTESIAN_POINT ( 'NONE',  ( -84.60374780145698992, -23.48786465467241413, 11.44779295918254469 ) ) ;
#37616=CARTESIAN_POINT ( 'NONE',  ( -20.46793573446543490, -22.99545800618565750, 10.97511746239722186 ) ) ;
#37617=CARTESIAN_POINT ( 'NONE',  ( 19.98943718749924159, -7.363913660680385220, -1.500000000000002220 ) ) ;
#37618=CARTESIAN_POINT ( 'NONE',  ( -55.62287095715006302, -23.48786465467240703, 11.44779295918255180 ) ) ;
#37619=CARTESIAN_POINT ( 'NONE',  ( -107.5179555912922922, -23.96169478059713853, 10.65365249895717348 ) ) ;
#37621=CARTESIAN_POINT ( 'NONE',  ( -85.62287095715005592, -24.14406661707769075, 10.28769366152060627 ) ) ;
#37622=CARTESIAN_POINT ( 'NONE',  ( -12.88509029660790617, -18.40938060607246740, -1.500000000000002220 ) ) ;
#37623=B_SPLINE_SURFACE_WITH_KNOTS ( 'NONE', 3, 1, ( 
 ( #18609, #4403 ),
 ( #20606, #11500 ),
 ( #49583, #74402 ),
 ( #3416, #59187 ),
 ( #96741, #35354 ),
 ( #96249, #57207 ),
 ( #73905, #34848 ),
 ( #42479, #66315 ),
 ( #27238, #89135 ),
 ( #80517, #19608 ),
 ( #50571, #28227 ),
 ( #41976, #81526 ),
 ( #51074, #12000 ),
 ( #72918, #12500 ),
 ( #43465, #4896 ) ),
 .UNSPECIFIED., .F., .F., .F.,
 ( 4, 1, 1, 1, 1, 1, 1, 1, 1, 1, 1, 1, 4 ),
 ( 2, 2 ),
 ( 0.000000000000000000, 0.08433472199262467828, 0.1670523184160704888, 0.2495660772409616646, 0.3327404818018447341, 0.4159148863627272763, 0.4978280095399966187, 0.5803725886080506324, 0.6646001210565021244, 0.7494666931126173770, 0.8325102339401406759, 0.9156392816681737656, 1.000000000000000000 ),
 ( 0.000000000000000000, 1.000000000000000000 ),
 .UNSPECIFIED. ) ;
#37624=CARTESIAN_POINT ( 'NONE',  ( -129.5228709571500474, -24.66019654487199730, 8.947790411086115725 ) ) ;
#37626=DIRECTION ( 'NONE',  ( 0.000000000000000000, -2.173523156925979552E-06, 0.9999999999976378895 ) ) ;
#37627=CARTESIAN_POINT ( 'NONE',  ( 13.16580039582533423, -14.52177825760336205, 11.49999999999999645 ) ) ;
#37629=LINE ( 'NONE', #90421, #2656 ) ;
#37630=ORIENTED_EDGE ( 'NONE', *, *, #65153, .F. ) ;
#37631=CARTESIAN_POINT ( 'NONE',  ( -69.67892052170711281, -25.30561282914882071, 4.980651892393407998 ) ) ;
#37632=CARTESIAN_POINT ( 'NONE',  ( -124.4728709571500360, -25.40558663563427189, 5.000950442582704270 ) ) ;
#37633=CARTESIAN_POINT ( 'NONE',  ( -100.5515626640960960, -25.25095778426572224, 5.205058283467153046 ) ) ;
#37635=CARTESIAN_POINT ( 'NONE',  ( -13.19171355488933983, -14.64934158388261665, -1.500000000000002220 ) ) ;
#37636=B_SPLINE_CURVE_WITH_KNOTS ( 'NONE', 3,
 ( #69071, #36132, #37621, #52852, #14772, #98009, #44252, #99995 ),
 .UNSPECIFIED., .F., .F.,
 ( 4, 2, 2, 4 ),
 ( 0.000000000000000000, 0.002001079623178217588, 0.003001619434767328117, 0.004002159246356438646 ),
 .UNSPECIFIED. ) ;
#37641=CARTESIAN_POINT ( 'NONE',  ( -110.3346797185884327, -25.19502912051678933, 3.293943094755625633 ) ) ;
#37646=CARTESIAN_POINT ( 'NONE',  ( -46.22287095715007155, -23.47593901973090880, -1.443836447538998424 ) ) ;
#37648=CARTESIAN_POINT ( 'NONE',  ( -55.59260180617345526, -24.40034930558990922, 0.3402023900116022959 ) ) ;
#37649=CARTESIAN_POINT ( 'NONE',  ( -99.33721417192995773, -25.26638451439988842, 7.148560506356232302 ) ) ;
#37650=DIRECTION ( 'NONE',  ( -1.000000000000000000, -3.773278334444166432E-23, -8.201307841325785021E-29 ) ) ;
#37651=FACE_OUTER_BOUND ( 'NONE', #59004, .T. ) ;
#37652=CARTESIAN_POINT ( 'NONE',  ( -107.5517470719624527, -24.34968618360934656, 0.1864209137778970737 ) ) ;
#37653=CARTESIAN_POINT ( 'NONE',  ( -7.473237707827510512, 18.53023608995856009, 11.49999999999998934 ) ) ;
#37654=EDGE_CURVE ( 'NONE', #49798, #20665, #8907, .T. ) ;
#37655=CARTESIAN_POINT ( 'NONE',  ( -107.6228709571500701, -29.50250243563736774, 8.947779886222136270 ) ) ;
#37656=CARTESIAN_POINT ( 'NONE',  ( -45.60106363764529647, -24.15602025860896163, 10.28564288303535434 ) ) ;
#37657=ORIENTED_EDGE ( 'NONE', *, *, #9439, .T. ) ;
#37660=CARTESIAN_POINT ( 'NONE',  ( -119.5880683731135719, -24.65952944569305316, 1.056160979905713226 ) ) ;
#37661=CARTESIAN_POINT ( 'NONE',  ( -112.5228709571500616, -23.47593901973090524, -1.443836447538996426 ) ) ;
#37663=CARTESIAN_POINT ( 'NONE',  ( -39.48050984162963317, -24.65952944569304250, 1.056160979905697017 ) ) ;
#37665=CARTESIAN_POINT ( 'NONE',  ( -51.61156992512332664, -25.31574345023019035, 4.398685571975743613 ) ) ;
#37667=FACE_OUTER_BOUND ( 'NONE', #18597, .T. ) ;
#37668=ORIENTED_EDGE ( 'NONE', *, *, #96759, .F. ) ;
#37669=CARTESIAN_POINT ( 'NONE',  ( -3.898967980886277829, 19.90457959416237088, -1.500000000000002220 ) ) ;
#37671=CARTESIAN_POINT ( 'NONE',  ( -54.52287095715005449, -23.47593901973090169, -1.443836447538997092 ) ) ;
#37673=CARTESIAN_POINT ( 'NONE',  ( -71.62287095715005592, -24.64965695001468404, 8.947790433994184056 ) ) ;
#37675=CARTESIAN_POINT ( 'NONE',  ( -77.52287095715006160, -23.47596703998600631, 11.44779298504228571 ) ) ;
#37678=CARTESIAN_POINT ( 'NONE',  ( -11.28321777122536140, 16.66956161807075887, -1.500000000000002220 ) ) ;
#37679=CARTESIAN_POINT ( 'NONE',  ( -16.00611555608923098, 13.71732778110762219, 11.49999999999999645 ) ) ;
#37680=DIRECTION ( 'NONE',  ( -3.773278334453079030E-23, 0.9999999999976377785, 2.173523156925979128E-06 ) ) ;
#37681=CARTESIAN_POINT ( 'NONE',  ( -2.366842300981895519, -21.98859952056468714, -1.500000000000002220 ) ) ;
#37682=EDGE_CURVE ( 'NONE', #87638, #64400, #73793, .T. ) ;
#37683=CARTESIAN_POINT ( 'NONE',  ( 15.21836549854886123, 13.79734045396011943, -1.500000000000002220 ) ) ;
#37684=CARTESIAN_POINT ( 'NONE',  ( -46.62287095715004881, -23.47596703998600276, 11.44779298504227505 ) ) ;
#37685=AXIS2_PLACEMENT_3D ( 'NONE', #18783, #63999, #78172 ) ;
#37690=CARTESIAN_POINT ( 'NONE',  ( -100.1132281341688639, -25.12645423365821529, 2.865483173913088599 ) ) ;
#37691=CARTESIAN_POINT ( 'NONE',  ( -94.62287095715005592, -29.50250786944525672, 11.44777988621623344 ) ) ;
#37692=ORIENTED_EDGE ( 'NONE', *, *, #86923, .T. ) ;
#37693=ORIENTED_EDGE ( 'NONE', *, *, #19138, .T. ) ;
#37695=CARTESIAN_POINT ( 'NONE',  ( -58.62287095715004881, -29.50250243563736774, 8.947779886222145151 ) ) ;
#37696=CARTESIAN_POINT ( 'NONE',  ( -71.62287095715005592, -24.64965695001468404, 8.947790433994184056 ) ) ;
#37697=CARTESIAN_POINT ( 'NONE',  ( -107.6228709571500701, -29.50247984919015209, -1.443849546365048253 ) ) ;
#37698=CARTESIAN_POINT ( 'NONE',  ( 19.88596897151998633, -5.565664080715476913, -1.500000000000002220 ) ) ;
#37699=CARTESIAN_POINT ( 'NONE',  ( -21.01067979154616694, 5.129389437380057259, 11.49999999999999645 ) ) ;
#37701=CARTESIAN_POINT ( 'NONE',  ( -83.52287095715006160, -29.50250243563736774, 8.947779886222141599 ) ) ;
#37703=CARTESIAN_POINT ( 'NONE',  ( -22.19192207843486386, -2.872123673023632584, -1.500000000000002220 ) ) ;
#37704=CARTESIAN_POINT ( 'NONE',  ( -34.52287095715006870, -23.96177878511308634, 10.65340807706330573 ) ) ;
#37705=CARTESIAN_POINT ( 'NONE',  ( -84.51365791126548288, -23.96119346886880663, -0.6495511937832096905 ) ) ;
#37706=EDGE_LOOP ( 'NONE', ( #45138, #42060, #33848, #34730 ) ) ;
#37707=CARTESIAN_POINT ( 'NONE',  ( -119.1719706626307413, -25.37174747607477698, 5.923220291595613141 ) ) ;
#37709=VECTOR ( 'NONE', #12926, 1000.000000000000114 ) ;
#37710=CARTESIAN_POINT ( 'NONE',  ( 19.40856703110355852, -7.758221025823637262, 11.49999999999998934 ) ) ;
#37711=ORIENTED_EDGE ( 'NONE', *, *, #30062, .F. ) ;
#37713=CARTESIAN_POINT ( 'NONE',  ( -67.64073919962002890, -23.96169478059713853, 10.65365249895717881 ) ) ;
#37714=ORIENTED_EDGE ( 'NONE', *, *, #41919, .F. ) ;
#37715=VERTEX_POINT ( 'NONE', #47980 ) ;
#37716=DIRECTION ( 'NONE',  ( -1.000000000000000000, -3.773278334444166432E-23, -8.201307841325785021E-29 ) ) ;
#37717=CARTESIAN_POINT ( 'NONE',  ( -1.424071398598787397, -21.11453822904667277, -1.500000000000002220 ) ) ;
#37718=ORIENTED_EDGE ( 'NONE', *, *, #71035, .F. ) ;
#37719=CARTESIAN_POINT ( 'NONE',  ( -117.5178561819711405, -24.34968618360934656, 0.1864209137778901071 ) ) ;
#37721=CARTESIAN_POINT ( 'NONE',  ( 21.67628855941699939, -2.339797445609365756, -1.500000000000002220 ) ) ;
#37722=CARTESIAN_POINT ( 'NONE',  ( -38.22287095715006444, -23.47596703998600276, 11.44779298504227683 ) ) ;
#37724=CARTESIAN_POINT ( 'NONE',  ( -51.70072539166533687, -29.50249165357793046, 3.987142867003085733 ) ) ;
#37725=CARTESIAN_POINT ( 'NONE',  ( -15.31764660673900558, 15.41647822393392175, -1.500000000000002220 ) ) ;
#37726=CARTESIAN_POINT ( 'NONE',  ( -79.23861220474265110, -25.15702039326336248, 6.966313354365812671 ) ) ;
#37727=CARTESIAN_POINT ( 'NONE',  ( -7.907391756136429528, -20.87048397725295956, 11.49999999999999645 ) ) ;
#37728=ORIENTED_EDGE ( 'NONE', *, *, #54196, .T. ) ;
#37729=CARTESIAN_POINT ( 'NONE',  ( -45.62287095715005592, -23.85196035786901447, -0.8779234886475056898 ) ) ;
#37730=CARTESIAN_POINT ( 'NONE',  ( -85.58227397182980667, -24.92592662359561473, 8.075495903018000021 ) ) ;
#37732=EDGE_LOOP ( 'NONE', ( #95844, #78560, #42260, #38570 ) ) ;
#37734=ORIENTED_EDGE ( 'NONE', *, *, #23633, .T. ) ;
#37735=VECTOR ( 'NONE', #42040, 1000.000000000000114 ) ;
#37736=EDGE_LOOP ( 'NONE', ( #43724, #3583, #92716, #22196 ) ) ;
#37738=CARTESIAN_POINT ( 'NONE',  ( -44.62287095715006302, -24.50216790748206108, 0.6166512839542489521 ) ) ;
#37739=CARTESIAN_POINT ( 'NONE',  ( 15.74494995282791088, 14.18698661492608615, 11.49999999999998934 ) ) ;
#37740=CARTESIAN_POINT ( 'NONE',  ( -42.62287095715004881, -24.64898659630367561, 1.056161002820819261 ) ) ;
#37741=CARTESIAN_POINT ( 'NONE',  ( -79.79245360944284471, -25.03138266959759406, 7.413205403593926768 ) ) ;
#37742=LINE ( 'NONE', #68702, #38911 ) ;
#37743=LINE ( 'NONE', #68704, #8638 ) ;
#37744=VECTOR ( 'NONE', #57399, 1000.000000000000114 ) ;
#37745=CARTESIAN_POINT ( 'NONE',  ( -37.62287095715005592, -23.48786465467240347, 11.44779295918255180 ) ) ;
#37746=CARTESIAN_POINT ( 'NONE',  ( -51.76059860518384426, -25.30455739459534215, 5.531002304556869476 ) ) ;
#37748=CARTESIAN_POINT ( 'NONE',  ( -19.27395093635484713, 2.380100695660296140, 11.49999999999999645 ) ) ;
#37751=EDGE_CURVE ( 'NONE', #11757, #25493, #98040, .T. ) ;
#37753=ORIENTED_EDGE ( 'NONE', *, *, #72315, .T. ) ;
#37756=B_SPLINE_CURVE_WITH_KNOTS ( 'NONE', 3,
 ( #86073, #16547, #47523, #336, #31282, #46026, #93175, #23662 ),
 .UNSPECIFIED., .F., .F.,
 ( 4, 2, 2, 4 ),
 ( 6.391158118953789392E-06, 0.002007136338672918345, 0.003007508928949900826, 0.004007881519226882440 ),
 .UNSPECIFIED. ) ;
#37758=CARTESIAN_POINT ( 'NONE',  ( -10.75157073690095721, 16.42123490324765811, 11.49999999999998934 ) ) ;
#37759=B_SPLINE_SURFACE_WITH_KNOTS ( 'NONE', 3, 3, ( 
 ( #73088, #27897, #58852, #66980 ),
 ( #51744, #44128, #57872, #88810 ),
 ( #19276, #50248, #14156, #61859 ),
 ( #67973, #68957, #68462, #60860 ) ),
 .UNSPECIFIED., .F., .F., .F.,
 ( 4, 4 ),
 ( 4, 4 ),
 ( 0.4256160872305289611, 0.5688882139226333345 ),
 ( 0.3941186795217973549, 0.4076941526734072507 ),
 .UNSPECIFIED. ) ;
#37760=CARTESIAN_POINT ( 'NONE',  ( -117.6228709571501128, -23.96177878511309345, 10.65340807706329507 ) ) ;
#37762=B_SPLINE_CURVE_WITH_KNOTS ( 'NONE', 3,
 ( #86794, #25400, #56375, #17286, #1577, #32010 ),
 .UNSPECIFIED., .F., .F.,
 ( 4, 2, 4 ),
 ( 6.391158118969316353E-06, 0.001387004593080788748, 0.002767618028042608501 ),
 .UNSPECIFIED. ) ;
#37763=CARTESIAN_POINT ( 'NONE',  ( -19.35566633068252074, -9.524217769563914970, 11.49999999999998934 ) ) ;
#37764=CARTESIAN_POINT ( 'NONE',  ( -33.53189478466186557, -24.51419770103157347, 9.386484678747185839 ) ) ;
#37765=CARTESIAN_POINT ( 'NONE',  ( -40.48180610888380926, -24.63355581998386512, 0.9682620441943814438 ) ) ;
#37766=CARTESIAN_POINT ( 'NONE',  ( -99.52818128268205555, -25.18439484051665644, 3.976272486753747781 ) ) ;
#37767=CARTESIAN_POINT ( 'NONE',  ( 14.79121776280621425, -17.69394282334246427, -1.500000000000002220 ) ) ;
#37768=EDGE_CURVE ( 'NONE', #72199, #81001, #24186, .T. ) ;
#37769=EDGE_CURVE ( 'NONE', #52694, #65117, #93194, .T. ) ;
#37771=CARTESIAN_POINT ( 'NONE',  ( -93.62357230945337960, -24.65952944569305316, 1.056160979905701458 ) ) ;
#37772=CARTESIAN_POINT ( 'NONE',  ( -89.52287095715006160, -23.47596703998600631, 11.44779298504228393 ) ) ;
#37773=CARTESIAN_POINT ( 'NONE',  ( -15.79248070760165490, 12.47733877207048181, 11.49999999999999645 ) ) ;
#37778=CARTESIAN_POINT ( 'NONE',  ( -31.52287095715006160, -23.47596703998600631, 11.44779298504229459 ) ) ;
#37779=CARTESIAN_POINT ( 'NONE',  ( 12.47747183659840786, 15.48776231947736015, -1.500000000000002220 ) ) ;
#37781=AXIS2_PLACEMENT_3D ( 'NONE', #50834, #43227, #81774 ) ;
#37782=CARTESIAN_POINT ( 'NONE',  ( -118.6228709571500701, -23.48786465467241769, 11.44779295918253759 ) ) ;
#37783=CARTESIAN_POINT ( 'NONE',  ( 19.51516567812286596, -3.327523070855789911, -1.500000000000002220 ) ) ;
#37784=CARTESIAN_POINT ( 'NONE',  ( -56.63816017806102820, -24.15543982623907127, -0.2315651400026670359 ) ) ;
#37785=EDGE_CURVE ( 'NONE', #71428, #35259, #26722, .T. ) ;
#37788=CARTESIAN_POINT ( 'NONE',  ( -39.04979701406145409, -25.10925853515279016, 4.033764255176815361 ) ) ;
#37790=CARTESIAN_POINT ( 'NONE',  ( -14.43086120294938368, -14.79396848081076854, 11.49999999999999645 ) ) ;
#37791=CARTESIAN_POINT ( 'NONE',  ( -56.52287095715005449, -23.47593901973090169, -1.443836447538996870 ) ) ;
#37792=CARTESIAN_POINT ( 'NONE',  ( -49.86018645952977835, -25.31439301394160779, 5.308912529311577977 ) ) ;
#37793=CARTESIAN_POINT ( 'NONE',  ( 22.03932947713327906, 5.445304565557160359, 11.49999999999999645 ) ) ;
#37794=B_SPLINE_CURVE_WITH_KNOTS ( 'NONE', 3,
 ( #42235, #64074, #88385, #33596, #73167, #47823, #79257, #56951, #64576, #25980, #86380, #9247, #40709, #72666, #10763, #40208, #94989, #71163 ),
 .UNSPECIFIED., .F., .F.,
 ( 4, 2, 2, 2, 2, 2, 2, 2, 4 ),
 ( 8.673617379884035472E-19, 0.0002908379182062560990, 0.0005816758364125113306, 0.0008725137546187665622, 0.001163351672825021794, 0.001454189591031277134, 0.001745027509237532257, 0.002035865427443787380, 0.002326703345650042720 ),
 .UNSPECIFIED. ) ;
#37795=ORIENTED_EDGE ( 'NONE', *, *, #100, .F. ) ;
#37797=CARTESIAN_POINT ( 'NONE',  ( -69.84645531399800689, -25.14135604393685952, 6.994270796255325884 ) ) ;
#37798=B_SPLINE_CURVE_WITH_KNOTS ( 'NONE', 3,
 ( #97547, #35662, #29028, #20405 ),
 .UNSPECIFIED., .F., .F.,
 ( 4, 4 ),
 ( 0.000000000000000000, 9.999999999998900014E-05 ),
 .UNSPECIFIED. ) ;
#37799=CARTESIAN_POINT ( 'NONE',  ( -20.16912494768211417, -0.3064379698199363733, -1.500000000000002220 ) ) ;
#37800=CARTESIAN_POINT ( 'NONE',  ( -63.60362512743664354, -23.73766607897669090, -1.055555164236456900 ) ) ;
#37801=PLANE ( 'NONE',  #20444 ) ;
#37802=VERTEX_POINT ( 'NONE', #35754 ) ;
#37803=VERTEX_POINT ( 'NONE', #58588 ) ;
#37805=CARTESIAN_POINT ( 'NONE',  ( 21.75204538223844963, -7.182240389990739438, 11.49999999999998934 ) ) ;
#37806=FACE_OUTER_BOUND ( 'NONE', #10023, .T. ) ;
#37807=CARTESIAN_POINT ( 'NONE',  ( -16.54959454218438708, 13.92943311328891554, -1.500000000000002220 ) ) ;
#37808=DIRECTION ( 'NONE',  ( 0.000000000000000000, 0.9999999999976377785, 2.173523156925979975E-06 ) ) ;
#37809=CARTESIAN_POINT ( 'NONE',  ( -43.62287095715004881, -29.50250243563736774, 8.947779886222148704 ) ) ;
#37810=CARTESIAN_POINT ( 'NONE',  ( -20.92377055399060737, -0.003182555231893603818, 11.49999999999999645 ) ) ;
#37811=VERTEX_POINT ( 'NONE', #66724 ) ;
#37812=CARTESIAN_POINT ( 'NONE',  ( -124.5557939318219667, -23.96119346886880663, -0.6495511937832024740 ) ) ;
#37813=CARTESIAN_POINT ( 'NONE',  ( -19.13726171168348245, 10.91495894028074432, 11.49999999999998934 ) ) ;
#37814=CARTESIAN_POINT ( 'NONE',  ( -105.5894839524365239, -24.52399227489126687, 9.353111116836517525 ) ) ;
#37815=CARTESIAN_POINT ( 'NONE',  ( -28.88518304243395818, -24.79700160504788542, 6.883447026959963466 ) ) ;
#37817=ORIENTED_EDGE ( 'NONE', *, *, #66132, .T. ) ;
#37819=CARTESIAN_POINT ( 'NONE',  ( -68.52287095715006160, -24.66019654487199730, 8.947790411086124607 ) ) ;
#37820=ORIENTED_EDGE ( 'NONE', *, *, #49507, .F. ) ;
#37821=CARTESIAN_POINT ( 'NONE',  ( -72.62362984840773095, -24.66019654487199730, 8.947790411086121054 ) ) ;
#37822=VERTEX_POINT ( 'NONE', #57602 ) ;
#37824=VERTEX_POINT ( 'NONE', #50477 ) ;
#37825=CARTESIAN_POINT ( 'NONE',  ( -71.58415216203414388, -24.51419770103159124, 9.386484678747166299 ) ) ;
#37826=CARTESIAN_POINT ( 'NONE',  ( -117.5562042904833504, -24.64965694238575011, 8.947790433994191162 ) ) ;
#37827=FACE_OUTER_BOUND ( 'NONE', #88202, .T. ) ;
#37828=CARTESIAN_POINT ( 'NONE',  ( -4.979992623568794130, 19.86841884474198494, -1.500000000000002220 ) ) ;
#37833=CARTESIAN_POINT ( 'NONE',  ( 16.16129659511371131, 15.28805624652528472, -1.500000000000002220 ) ) ;
#37835=DIRECTION ( 'NONE',  ( -3.773278334453079618E-23, 0.9999999999976377785, 2.173523156925979975E-06 ) ) ;
#37838=CARTESIAN_POINT ( 'NONE',  ( -64.52287095715006160, -23.48786465467241769, 11.44779295918254824 ) ) ;
#37839=CARTESIAN_POINT ( 'NONE',  ( 19.92439739378097840, -5.974006126113303949, -1.500000000000002220 ) ) ;
#37840=ORIENTED_EDGE ( 'NONE', *, *, #73316, .F. ) ;
#37841=CARTESIAN_POINT ( 'NONE',  ( -42.52287095715005449, -24.66019654487199020, 8.947790411086133489 ) ) ;
#37843=EDGE_CURVE ( 'NONE', #37096, #36594, #66224, .T. ) ;
#37844=B_SPLINE_SURFACE_WITH_KNOTS ( 'NONE', 3, 1, ( 
 ( #79786, #55467 ),
 ( #2188, #71189 ),
 ( #2684, #47850 ),
 ( #10284, #41240 ),
 ( #26005, #78772 ),
 ( #9272, #40237 ),
 ( #74184, #81794 ),
 ( #66102, #49869 ),
 ( #35628, #89906 ),
 ( #34130, #57978 ),
 ( #88917, #3683 ) ),
 .UNSPECIFIED., .F., .F., .F.,
 ( 4, 1, 1, 1, 1, 1, 1, 1, 4 ),
 ( 2, 2 ),
 ( 0.000000000000000000, 0.1281581855276738569, 0.2536731361531681661, 0.3773253059734874015, 0.4993845547646074690, 0.6229183680423439062, 0.7458393931045753655, 0.8713952850140305184, 1.000000000000000000 ),
 ( 0.000000000000000000, 1.000000000000000000 ),
 .UNSPECIFIED. ) ;
#37845=CARTESIAN_POINT ( 'NONE',  ( -31.58953762381672092, -24.65952944569304606, 1.056160979905695907 ) ) ;
#37846=ORIENTED_EDGE ( 'NONE', *, *, #17308, .F. ) ;
#37847=ORIENTED_EDGE ( 'NONE', *, *, #12411, .F. ) ;
#37850=CARTESIAN_POINT ( 'NONE',  ( -116.4728709571500360, -25.30558663486635140, 5.000950659935019971 ) ) ;
#37851=EDGE_CURVE ( 'NONE', #7232, #49833, #83489, .T. ) ;
#37852=CARTESIAN_POINT ( 'NONE',  ( -115.5228709571500616, -29.50250243563736774, 8.947779886222134493 ) ) ;
#37853=CARTESIAN_POINT ( 'NONE',  ( -108.9545715455114987, -25.28708312187852414, 4.170144817753115518 ) ) ;
#37854=CARTESIAN_POINT ( 'NONE',  ( -95.58953762381672448, -23.47596703998600631, 11.44779298504227683 ) ) ;
#37855=CARTESIAN_POINT ( 'NONE',  ( 22.15222936869060177, 0.07132910108538677296, 11.49999999999999645 ) ) ;
#37856=ORIENTED_EDGE ( 'NONE', *, *, #92509, .T. ) ;
#37857=CARTESIAN_POINT ( 'NONE',  ( -91.94687923781920347, -25.22391124735684187, 6.409327647371628522 ) ) ;
#37858=CARTESIAN_POINT ( 'NONE',  ( -1.322449806865925614, 22.60218017400935864, -1.500000000000002220 ) ) ;
#37862=CARTESIAN_POINT ( 'NONE',  ( -87.62287095715004170, -23.47593901973091235, -1.443836447539002865 ) ) ;
#37864=AXIS2_PLACEMENT_3D ( 'NONE', #21259, #52233, #75544 ) ;
#37867=CARTESIAN_POINT ( 'NONE',  ( -113.5228709571500616, -23.47596703998600631, 11.44779298504228038 ) ) ;
#37868=CARTESIAN_POINT ( 'NONE',  ( -19.68739882612603864, 4.164723872966736629, -1.500000000000002220 ) ) ;
#37869=CARTESIAN_POINT ( 'NONE',  ( -99.62287095715005592, -23.47596703998600631, 11.44779298504227860 ) ) ;
#37872=CARTESIAN_POINT ( 'NONE',  ( -10.28394192611005842, 19.82837715243953625, -1.500000000000002220 ) ) ;
#37873=EDGE_CURVE ( 'NONE', #97847, #38686, #65612, .T. ) ;
#37876=EDGE_LOOP ( 'NONE', ( #61491, #15411, #47408, #22841 ) ) ;
#37878=CARTESIAN_POINT ( 'NONE',  ( -119.5562042904834072, -23.48786465467241769, 11.44779295918253759 ) ) ;
#37879=CARTESIAN_POINT ( 'NONE',  ( -80.53842267555941703, -25.29579208320836869, 4.514328772014316371 ) ) ;
#37880=DIRECTION ( 'NONE',  ( 1.000000000000000000, 3.773278334444166432E-23, 8.201307841325785021E-29 ) ) ;
#37882=CARTESIAN_POINT ( 'NONE',  ( 17.37147561666312257, 8.948746033654231269, 11.49999999999998934 ) ) ;
#37884=CARTESIAN_POINT ( 'NONE',  ( -5.860608850286626925, 20.67097946995454905, 11.49999999999998934 ) ) ;
#37885=CARTESIAN_POINT ( 'NONE',  ( -25.89225704477708589, -24.57999767617803855, 2.873802903271038822 ) ) ;
#37886=DIRECTION ( 'NONE',  ( -3.773278334444166432E-23, 1.000000000000000000, 0.000000000000000000 ) ) ;
#37887=CARTESIAN_POINT ( 'NONE',  ( -64.62287095715007013, -23.47596703998600631, 11.44779298504227683 ) ) ;
#37888=CARTESIAN_POINT ( 'NONE',  ( -16.32851894532483783, 16.03542138455653898, -1.500000000000002220 ) ) ;
#37892=CARTESIAN_POINT ( 'NONE',  ( -45.62287095715004881, -29.50248528299804818, 1.056150453629033370 ) ) ;
#37894=CARTESIAN_POINT ( 'NONE',  ( 18.25133680241413359, 8.160682379734268466, 11.49999999999999645 ) ) ;
#37895=DIRECTION ( 'NONE',  ( 0.000000000000000000, -0.9999999999976377785, -2.173523156925979128E-06 ) ) ;
#37897=CARTESIAN_POINT ( 'NONE',  ( -74.52211788372726176, -23.48786465467241058, 11.44779295918254824 ) ) ;
#37898=DIRECTION ( 'NONE',  ( -1.000000000000000000, -3.773278334444167020E-23, -8.201307838832447938E-29 ) ) ;
#37900=CARTESIAN_POINT ( 'NONE',  ( -83.52287095715007581, -23.96177878511310055, 10.65340807706330217 ) ) ;
#37902=CARTESIAN_POINT ( 'NONE',  ( 18.07971092720299922, 12.08445254275838465, 11.49999999999998934 ) ) ;
#37903=CARTESIAN_POINT ( 'NONE',  ( -56.62287095715005592, -23.73934037231757443, 11.05740245334328797 ) ) ;
#37904=CARTESIAN_POINT ( 'NONE',  ( 2.036066721924049805, 19.47704226162102614, -1.500000000000002220 ) ) ;
#37905=FACE_OUTER_BOUND ( 'NONE', #54821, .T. ) ;
#37909=CARTESIAN_POINT ( 'NONE',  ( -104.6228709571500559, -23.47593901973091235, -1.443836447539001089 ) ) ;
#37911=CARTESIAN_POINT ( 'NONE',  ( 3.385237411341575964, -20.22741857368478335, 11.49999999999999645 ) ) ;
#37913=B_SPLINE_CURVE_WITH_KNOTS ( 'NONE', 3,
 ( #40631, #63484, #2570, #33511 ),
 .UNSPECIFIED., .F., .F.,
 ( 4, 4 ),
 ( 0.000000000000000000, 9.999999999999592548E-05 ),
 .UNSPECIFIED. ) ;
#37917=CARTESIAN_POINT ( 'NONE',  ( -30.47287095715007510, -23.47596703474403768, 11.44538124590455830 ) ) ;
#37919=CARTESIAN_POINT ( 'NONE',  ( -125.5899142108936672, -24.40133493613050675, 9.663955038902798833 ) ) ;
#37921=LINE ( 'NONE', #60276, #43563 ) ;
#37922=CARTESIAN_POINT ( 'NONE',  ( -42.62287095715006302, -23.47596703998600276, 11.44779298504227505 ) ) ;
#37923=CARTESIAN_POINT ( 'NONE',  ( 6.753845092018655016, 22.03294598498517232, 11.49999999999999645 ) ) ;
#37924=CARTESIAN_POINT ( 'NONE',  ( -7.756741253720922380, -21.46081514045699024, 11.49999999999998934 ) ) ;
#37925=CARTESIAN_POINT ( 'NONE',  ( -29.52287095715007581, -24.57618165405973087, 1.056161296257514870 ) ) ;
#37926=AXIS2_PLACEMENT_3D ( 'NONE', #3272, #43813, #12350 ) ;
#37928=CARTESIAN_POINT ( 'NONE',  ( -57.52287095715005449, -24.50216790748204687, 0.6166512839542507285 ) ) ;
#37929=CARTESIAN_POINT ( 'NONE',  ( -40.52287095715007581, -24.63345952396255356, 9.038047939301511846 ) ) ;
#37930=CARTESIAN_POINT ( 'NONE',  ( -110.5501846981437239, -24.73486907724917572, 1.287355809206965240 ) ) ;
#37931=CARTESIAN_POINT ( 'NONE',  ( 21.14253370195585546, 5.708146584608840612, 11.49999999999998934 ) ) ;
#37932=CARTESIAN_POINT ( 'NONE',  ( -38.52287095715006870, -24.66019654487199730, 8.947790411086121054 ) ) ;
#37933=CARTESIAN_POINT ( 'NONE',  ( -87.56249327518180792, -23.48786465467240703, 11.44779295918254647 ) ) ;
#37935=CARTESIAN_POINT ( 'NONE',  ( -36.52287095715006870, -29.50250786944525672, 11.44777988621624232 ) ) ;
#37936=CARTESIAN_POINT ( 'NONE',  ( -115.5228709571500616, -29.50247984919015209, -1.443849546365046699 ) ) ;
#37938=CARTESIAN_POINT ( 'NONE',  ( 5.749347661499963458, 19.61174949527739386, 11.49999999999998934 ) ) ;
#37939=ORIENTED_EDGE ( 'NONE', *, *, #70538, .F. ) ;
#37940=VERTEX_POINT ( 'NONE', #61816 ) ;
#37941=EDGE_LOOP ( 'NONE', ( #48731, #9658, #90618, #49326 ) ) ;
#37943=CARTESIAN_POINT ( 'NONE',  ( 11.92049557817732364, -19.74369927386287671, 11.49999999999998934 ) ) ;
#37944=CARTESIAN_POINT ( 'NONE',  ( -61.54325905924635265, -24.34968618360933945, 0.1864209137778810865 ) ) ;
#37945=CARTESIAN_POINT ( 'NONE',  ( -0.5548696950099620828, -20.20177982057877841, -1.500000000000002220 ) ) ;
#37947=CARTESIAN_POINT ( 'NONE',  ( -27.14406549058544726, -24.94612812924882661, 6.759032221908315208 ) ) ;
#37949=B_SPLINE_CURVE_WITH_KNOTS ( 'NONE', 3,
 ( #61048, #132, #85361, #91980, #52433, #37696 ),
 .UNSPECIFIED., .F., .F.,
 ( 4, 2, 4 ),
 ( 0.000000000000000000, 0.001380901958385383124, 0.002761803916770766247 ),
 .UNSPECIFIED. ) ;
#37950=FACE_OUTER_BOUND ( 'NONE', #46448, .T. ) ;
#37951=CARTESIAN_POINT ( 'NONE',  ( -70.63481881909494575, -24.52300882791528380, 0.6510814631126248253 ) ) ;
#37952=CARTESIAN_POINT ( 'NONE',  ( 1.049947104896167049, -21.43676768134831434, 11.49999999999999645 ) ) ;
#37953=ORIENTED_EDGE ( 'NONE', *, *, #78761, .T. ) ;
#37954=CARTESIAN_POINT ( 'NONE',  ( -113.6228709571500275, -24.33832256526968862, 0.1851278514119947260 ) ) ;
#37955=CARTESIAN_POINT ( 'NONE',  ( -111.2228709571500502, -23.47593901973090524, -1.443836447538996426 ) ) ;
#37956=B_SPLINE_CURVE_WITH_KNOTS ( 'NONE', 3,
 ( #67219, #5796, #74316, #59599 ),
 .UNSPECIFIED., .F., .F.,
 ( 4, 4 ),
 ( 0.000000000000000000, 9.999999999997510880E-05 ),
 .UNSPECIFIED. ) ;
#37958=CARTESIAN_POINT ( 'NONE',  ( 18.07348078632662691, -10.09602009226539288, 11.49999999999998934 ) ) ;
#37960=CARTESIAN_POINT ( 'NONE',  ( -123.6228709571500559, -24.65952944569304961, 1.056160979905703234 ) ) ;
#37961=ORIENTED_EDGE ( 'NONE', *, *, #56811, .T. ) ;
#37964=ORIENTED_EDGE ( 'NONE', *, *, #35921, .F. ) ;
#37967=EDGE_CURVE ( 'NONE', #9703, #93197, #70439, .T. ) ;
#37968=CARTESIAN_POINT ( 'NONE',  ( -65.57896445802249730, -24.92564183028979130, 1.928384488918254869 ) ) ;
#37969=CARTESIAN_POINT ( 'NONE',  ( 5.346615758220810477, 21.33151429383102382, 11.49999999999999645 ) ) ;
#37972=CARTESIAN_POINT ( 'NONE',  ( 17.82461400791848405, -13.82690402418615960, 11.49999999999998934 ) ) ;
#37974=CARTESIAN_POINT ( 'NONE',  ( -18.73635099073748833, 9.434554061794083069, -1.500000000000002220 ) ) ;
#37975=CARTESIAN_POINT ( 'NONE',  ( -109.8650237084402619, -25.29042187987247914, 5.784623108531866897 ) ) ;
#37976=EDGE_CURVE ( 'NONE', #76909, #79516, #19567, .T. ) ;
#37978=ORIENTED_EDGE ( 'NONE', *, *, #80306, .F. ) ;
#37980=ADVANCED_FACE ( 'NONE', ( #69415 ), #92736, .F. ) ;
#37981=VERTEX_POINT ( 'NONE', #26243 ) ;
#37982=CARTESIAN_POINT ( 'NONE',  ( -88.52287095715006160, -23.47596703998600631, 11.44779298504228393 ) ) ;
#37984=CARTESIAN_POINT ( 'NONE',  ( -21.46803524902295024, 1.580295693706654347, -1.500000000000002220 ) ) ;
#37985=B_SPLINE_CURVE_WITH_KNOTS ( 'NONE', 3,
 ( #97114, #38193, #16357, #31080, #84872, #99580, #92977, #38695 ),
 .UNSPECIFIED., .F., .F.,
 ( 4, 2, 2, 4 ),
 ( 0.000000000000000000, 0.002001098010032681049, 0.003001647015049021573, 0.004002196020065362098 ),
 .UNSPECIFIED. ) ;
#37988=CARTESIAN_POINT ( 'NONE',  ( -15.95541298346445735, 13.85296639876547076, -1.500000000000002220 ) ) ;
#37990=CARTESIAN_POINT ( 'NONE',  ( -64.53586813036071135, -24.65952944569304250, 1.056160979905695685 ) ) ;
#37991=CARTESIAN_POINT ( 'NONE',  ( -50.28147435909711049, -25.30259094565539257, 4.732480668705053795 ) ) ;
#37994=CARTESIAN_POINT ( 'NONE',  ( -2.513997614918375589, -22.02279109229760223, -1.500000000000002220 ) ) ;
#37995=CARTESIAN_POINT ( 'NONE',  ( -114.6307832717401851, -23.48783264082478794, -1.443836473390062380 ) ) ;
#37999=CARTESIAN_POINT ( 'NONE',  ( -51.15602047325173629, -25.31633097224522189, 4.998862860385179907 ) ) ;
#38001=CARTESIAN_POINT ( 'NONE',  ( -83.62287095715005592, -23.47593901973091235, -1.443836447539004642 ) ) ;
#38003=ADVANCED_FACE ( 'NONE', ( #2922 ), #2835, .T. ) ;
#38004=CARTESIAN_POINT ( 'NONE',  ( 12.19879910451502703, -15.15100395215988449, -1.500000000000002220 ) ) ;
#38005=CARTESIAN_POINT ( 'NONE',  ( -17.20161093224466953, -12.68000408521323408, 11.49999999999998934 ) ) ;
#38007=CARTESIAN_POINT ( 'NONE',  ( -124.5228709571500616, -24.64965694238575722, 8.947790433994191162 ) ) ;
#38010=CARTESIAN_POINT ( 'NONE',  ( -4.086358941109507370, -22.34742993483353146, -1.500000000000002220 ) ) ;
#38011=EDGE_LOOP ( 'NONE', ( #69673, #3326, #43578, #70918 ) ) ;
#38012=CARTESIAN_POINT ( 'NONE',  ( -58.52287095715006160, -24.64965694238407323, 8.947790433994201820 ) ) ;
#38013=CARTESIAN_POINT ( 'NONE',  ( -57.62287095715001328, -24.35013146730203459, 9.818937971375111928 ) ) ;
#38014=CARTESIAN_POINT ( 'NONE',  ( -10.52764212615999639, 16.74383705166681580, 11.49999999999999645 ) ) ;
#38015=CARTESIAN_POINT ( 'NONE',  ( -117.5228709571500758, -29.50248528299804818, 1.056150453629045360 ) ) ;
#38016=EDGE_LOOP ( 'NONE', ( #89741, #15947, #89625, #70532 ) ) ;
#38017=CARTESIAN_POINT ( 'NONE',  ( -48.62287095715004881, -23.48783264082478439, -1.443836473390070596 ) ) ;
#38018=CARTESIAN_POINT ( 'NONE',  ( -87.52287095715006160, -23.47596703998600631, 11.44779298504228393 ) ) ;
#38019=CARTESIAN_POINT ( 'NONE',  ( 19.51036611237648088, 9.378288983258578071, -1.500000000000002220 ) ) ;
#38020=CARTESIAN_POINT ( 'NONE',  ( -45.52287095715004739, -23.48783264082477018, -1.443836473390097019 ) ) ;
#38021=CARTESIAN_POINT ( 'NONE',  ( 15.36829964806744364, -11.83880051060199712, -1.500000000000002220 ) ) ;
#38022=CARTESIAN_POINT ( 'NONE',  ( -82.52287095715007581, -23.96177878511308634, 10.65340807706329862 ) ) ;
#38024=EDGE_CURVE ( 'NONE', #81873, #83477, #32348, .T. ) ;
#38025=CARTESIAN_POINT ( 'NONE',  ( 19.71268880909926580, -1.816447362451163450, 11.49999999999998934 ) ) ;
#38026=ORIENTED_EDGE ( 'NONE', *, *, #38290, .F. ) ;
#38028=CARTESIAN_POINT ( 'NONE',  ( 9.809556900635294951, 17.81656380412256269, 11.49999999999999645 ) ) ;
#38029=CARTESIAN_POINT ( 'NONE',  ( -118.5228709571500758, -29.50250786944525672, 11.44777988621622811 ) ) ;
#38030=EDGE_CURVE ( 'NONE', #32620, #11368, #86637, .T. ) ;
#38032=VERTEX_POINT ( 'NONE', #1914 ) ;
#38033=B_SPLINE_SURFACE_WITH_KNOTS ( 'NONE', 3, 3, ( 
 ( #45454, #76859, #45948, #23073 ),
 ( #37338, #37825, #84493, #77862 ),
 ( #21585, #68778, #52557, #54064 ),
 ( #29713, #7360, #84988, #7866 ),
 ( #8369, #92595, #62675, #99696 ),
 ( #46434, #30200, #62172, #69273 ),
 ( #93095, #23578, #54548, #92104 ) ),
 .UNSPECIFIED., .F., .F., .F.,
 ( 4, 3, 4 ),
 ( 4, 4 ),
 ( 0.7945040050992235869, 0.8970133687736498995, 0.9995227324480762121 ),
 ( 0.5896438339135527951, 0.5909287771905322728 ),
 .UNSPECIFIED. ) ;
#38034=CARTESIAN_POINT ( 'NONE',  ( -30.59800378598952264, -24.75991027412950274, 1.063373454495736947 ) ) ;
#38035=CARTESIAN_POINT ( 'NONE',  ( -119.4728709571500502, -25.21147115889350587, 5.000950862241205996 ) ) ;
#38038=CARTESIAN_POINT ( 'NONE',  ( -127.6228709571500559, -24.50321055353805377, 9.387540953477520489 ) ) ;
#38039=CARTESIAN_POINT ( 'NONE',  ( -16.07871291144651593, -12.00523380332558965, 11.49999999999998934 ) ) ;
#38040=CARTESIAN_POINT ( 'NONE',  ( -109.6228709571500417, -23.48786465467242124, 11.44779295918253936 ) ) ;
#38043=CARTESIAN_POINT ( 'NONE',  ( -12.73177969873712279, -19.06072230859735939, 11.49999999999999645 ) ) ;
#38044=CARTESIAN_POINT ( 'NONE',  ( -14.94938274637043207, -17.11189489004485864, 11.49999999999998934 ) ) ;
#38046=CARTESIAN_POINT ( 'NONE',  ( -29.62287095715004881, -29.50248298729119867, -6.412432996800796609E-05 ) ) ;
#38047=CARTESIAN_POINT ( 'NONE',  ( -38.61777322412189051, -23.48786465467240347, 11.44779295918255002 ) ) ;
#38052=ORIENTED_EDGE ( 'NONE', *, *, #64244, .T. ) ;
#38053=CARTESIAN_POINT ( 'NONE',  ( 8.194921280291850962, -18.63391395107102610, 11.49999999999998934 ) ) ;
#38054=ORIENTED_EDGE ( 'NONE', *, *, #35140, .F. ) ;
#38055=CARTESIAN_POINT ( 'NONE',  ( -18.50152239663938403, 13.63810111590111163, -1.500000000000002220 ) ) ;
#38056=CARTESIAN_POINT ( 'NONE',  ( -53.52287095715004739, -24.35013146730203815, 9.818937971375104823 ) ) ;
#38059=CARTESIAN_POINT ( 'NONE',  ( -101.6228709571500985, -23.95044443724992789, 10.65354141964649592 ) ) ;
#38060=CARTESIAN_POINT ( 'NONE',  ( -77.50832112164282250, -24.15620529776628800, 10.23563542870659937 ) ) ;
#38061=CARTESIAN_POINT ( 'NONE',  ( -40.62287095715004170, -24.99132157543083466, 2.256160258750667502 ) ) ;
#38062=CARTESIAN_POINT ( 'NONE',  ( -12.14505723179402530, 17.47690347785001919, 11.49999999999999645 ) ) ;
#38063=ORIENTED_EDGE ( 'NONE', *, *, #48818, .F. ) ;
#38064=ORIENTED_EDGE ( 'NONE', *, *, #11411, .T. ) ;
#38065=CARTESIAN_POINT ( 'NONE',  ( 19.86420646539740176, -9.926203236129387264, -1.500000000000002220 ) ) ;
#38066=CARTESIAN_POINT ( 'NONE',  ( -3.146292006899429783, -20.37002610441940220, 11.49999999999998934 ) ) ;
#38068=VERTEX_POINT ( 'NONE', #94746 ) ;
#38069=EDGE_CURVE ( 'NONE', #90203, #94029, #267, .T. ) ;
#38070=CARTESIAN_POINT ( 'NONE',  ( -109.0556427821970260, -25.27682694363410576, 4.716568693008002633 ) ) ;
#38071=CARTESIAN_POINT ( 'NONE',  ( -121.6228709571500985, -24.51283580621365488, 0.6167428607019845854 ) ) ;
#38076=CARTESIAN_POINT ( 'NONE',  ( -39.52287095715006870, -23.47596703998600631, 11.44779298504229281 ) ) ;
#38077=CARTESIAN_POINT ( 'NONE',  ( -35.58953762381672448, -23.48786465467240347, 11.44779295918255180 ) ) ;
#38078=CARTESIAN_POINT ( 'NONE',  ( 20.75994597877129877, -1.272245555857973054, -1.500000000000002220 ) ) ;
#38079=CARTESIAN_POINT ( 'NONE',  ( -5.167225684058948332, 21.16526716281445530, 11.49999999999999645 ) ) ;
#38080=ADVANCED_FACE ( 'NONE', ( #59197 ), #20614, .F. ) ;
#38081=CARTESIAN_POINT ( 'NONE',  ( -40.20787662131280626, -25.18822154510203148, 3.317274650640859690 ) ) ;
#38083=CARTESIAN_POINT ( 'NONE',  ( -18.83616483605274539, -12.25834331966736102, 11.49999999999998934 ) ) ;
#38086=EDGE_LOOP ( 'NONE', ( #96112, #16299, #23420, #63737 ) ) ;
#38088=CARTESIAN_POINT ( 'NONE',  ( -101.6814946224345704, -25.24282061761981311, 6.236250683194342059 ) ) ;
#38091=ORIENTED_EDGE ( 'NONE', *, *, #35448, .F. ) ;
#38092=ADVANCED_FACE ( 'NONE', ( #89144 ), #19618, .T. ) ;
#38094=ORIENTED_EDGE ( 'NONE', *, *, #10524, .T. ) ;
#38095=CARTESIAN_POINT ( 'NONE',  ( -17.73838780825237649, 11.93509662624355450, -1.500000000000002220 ) ) ;
#38096=ORIENTED_EDGE ( 'NONE', *, *, #79311, .T. ) ;
#38097=CARTESIAN_POINT ( 'NONE',  ( -19.40065202112720755, 8.109199488025859992, 11.49999999999998934 ) ) ;
#38098=CARTESIAN_POINT ( 'NONE',  ( -30.52453496278478084, -25.14632053279673585, 2.712646531854225440 ) ) ;
#38100=CARTESIAN_POINT ( 'NONE',  ( -110.3346797185884327, -25.19502912051678933, 3.293943094755625633 ) ) ;
#38101=CARTESIAN_POINT ( 'NONE',  ( -65.52287095715009002, -23.84081130425358808, 10.88220057483157888 ) ) ;
#38102=CARTESIAN_POINT ( 'NONE',  ( 21.52718982488130450, -4.553922534329950089, -1.500000000000002220 ) ) ;
#38104=ORIENTED_EDGE ( 'NONE', *, *, #66061, .F. ) ;
#38105=CARTESIAN_POINT ( 'NONE',  ( -38.92287095715006018, -23.47593901973090524, -1.443836447538997980 ) ) ;
#38106=FACE_OUTER_BOUND ( 'NONE', #36083, .T. ) ;
#38109=CARTESIAN_POINT ( 'NONE',  ( -0.02085506613324685302, -22.78001478014107306, 7.291654623549817416 ) ) ;
#38110=CARTESIAN_POINT ( 'NONE',  ( 19.49461108348020133, 8.573440864381753457, -1.500000000000002220 ) ) ;
#38111=CARTESIAN_POINT ( 'NONE',  ( -98.55250113363597109, -24.15620529776628445, 10.23563542870660292 ) ) ;
#38112=CARTESIAN_POINT ( 'NONE',  ( -107.5517401469810324, -24.35071581493543746, 9.817618358456021710 ) ) ;
#38115=CARTESIAN_POINT ( 'NONE',  ( -33.58674611195124982, -24.34968618360933235, 0.1864209137778845560 ) ) ;
#38116=CARTESIAN_POINT ( 'NONE',  ( 9.993301969596378953, 20.15287186522775542, -1.500000000000002220 ) ) ;
#38117=CARTESIAN_POINT ( 'NONE',  ( -111.9710651877489767, -25.32390614315827193, 4.358500768180118889 ) ) ;
#38119=FACE_OUTER_BOUND ( 'NONE', #87911, .T. ) ;
#38120=CARTESIAN_POINT ( 'NONE',  ( 10.60981200654714307, 16.52409317135366607, 11.49999999999999645 ) ) ;
#38121=CARTESIAN_POINT ( 'NONE',  ( -125.6228709571500559, -24.92579138211019085, 1.929029949965666457 ) ) ;
#38122=CARTESIAN_POINT ( 'NONE',  ( -82.52287095715006160, -24.65952944569304606, 1.056160979905698794 ) ) ;
#38125=CARTESIAN_POINT ( 'NONE',  ( -88.51806219836213074, -23.73791477778912196, 11.05961554403170588 ) ) ;
#38126=CARTESIAN_POINT ( 'NONE',  ( -127.2834360451832225, -25.38371582119480507, 5.756550691135934095 ) ) ;
#38127=CARTESIAN_POINT ( 'NONE',  ( -100.4277023991755442, -25.31439536995993933, 5.215800341084221081 ) ) ;
#38128=AXIS2_PLACEMENT_3D ( 'NONE', #2267, #34706, #41320 ) ;
#38129=CARTESIAN_POINT ( 'NONE',  ( -10.60818629614422370, 16.63341085705455669, 11.49999999999998934 ) ) ;
#38130=EDGE_LOOP ( 'NONE', ( #3699, #14245, #76773, #81199 ) ) ;
#38136=EDGE_LOOP ( 'NONE', ( #62421, #14184, #9506, #72626 ) ) ;
#38137=CARTESIAN_POINT ( 'NONE',  ( -96.58953762381672448, -24.64898659630368272, 1.056161002820388273 ) ) ;
#38141=CARTESIAN_POINT ( 'NONE',  ( -66.62287095715005592, -24.64965695001468404, 8.947790433994184056 ) ) ;
#38143=CARTESIAN_POINT ( 'NONE',  ( -107.5116988131331084, -24.65952944569305316, 1.056160979905704789 ) ) ;
#38144=CARTESIAN_POINT ( 'NONE',  ( -8.876215969300202957, 17.89991547088461488, -1.500000000000002220 ) ) ;
#38145=CARTESIAN_POINT ( 'NONE',  ( -127.6228709571500559, -23.94994826722515668, -0.6494450866351666463 ) ) ;
#38146=CARTESIAN_POINT ( 'NONE',  ( -45.52251258058822714, -25.00182538069146787, 7.747789668545044250 ) ) ;
#38148=CARTESIAN_POINT ( 'NONE',  ( -119.5539613361492144, -24.34968618360934656, 0.1864209137778924941 ) ) ;
#38149=AXIS2_PLACEMENT_3D ( 'NONE', #30171, #69241, #61151 ) ;
#38150=CARTESIAN_POINT ( 'NONE',  ( -80.54343777448522701, -24.63419186844610920, 9.035850630976922204 ) ) ;
#38152=CARTESIAN_POINT ( 'NONE',  ( -108.5228709571500758, -23.94994826722565762, -0.6494450866342741380 ) ) ;
#38156=CARTESIAN_POINT ( 'NONE',  ( -37.62287095715007723, -23.72773821059535493, 11.05748984161097503 ) ) ;
#38159=B_SPLINE_CURVE_WITH_KNOTS ( 'NONE', 3,
 ( #83542, #51611, #90661, #28767 ),
 .UNSPECIFIED., .F., .F.,
 ( 4, 4 ),
 ( 0.000000000000000000, 0.0001000000000000028644 ),
 .UNSPECIFIED. ) ;
#38160=CARTESIAN_POINT ( 'NONE',  ( 0.7435384974594729801, 20.27106041150680937, -1.500000000000002220 ) ) ;
#38161=CARTESIAN_POINT ( 'NONE',  ( -122.5195476943700186, -24.34968618360934300, 0.1864209137778895797 ) ) ;
#38163=DIRECTION ( 'NONE',  ( -3.773278334453079030E-23, 0.9999999999976377785, 2.173523156925979128E-06 ) ) ;
#38165=CARTESIAN_POINT ( 'NONE',  ( -73.62287095715005592, -29.50250786944525672, 11.44777988621623699 ) ) ;
#38166=CARTESIAN_POINT ( 'NONE',  ( 13.10547390533899836, 15.29217475743441312, -1.500000000000002220 ) ) ;
#38167=CARTESIAN_POINT ( 'NONE',  ( -14.29351441246084065, -15.47709782942846424, 11.49999999999999645 ) ) ;
#38168=LINE ( 'NONE', #14331, #62846 ) ;
#38169=CARTESIAN_POINT ( 'NONE',  ( 21.80885565983754404, 3.581153529568561478, 11.49999999999998934 ) ) ;
#38170=CARTESIAN_POINT ( 'NONE',  ( 18.67943556539783856, 8.552475402716291697, 11.49999999999998934 ) ) ;
#38171=CARTESIAN_POINT ( 'NONE',  ( -60.85008211737284256, -25.20813793428145289, 6.796440242136131182 ) ) ;
#38172=VECTOR ( 'NONE', #73034, 1000.000000000000114 ) ;
#38173=CARTESIAN_POINT ( 'NONE',  ( -60.50382013959431049, -24.15503026093916006, -0.2815557561904390993 ) ) ;
#38174=ORIENTED_EDGE ( 'NONE', *, *, #84884, .T. ) ;
#38175=LINE ( 'NONE', #28581, #10409 ) ;
#38176=ORIENTED_EDGE ( 'NONE', *, *, #1587, .T. ) ;
#38178=DIRECTION ( 'NONE',  ( -3.773278334444167608E-23, 1.000000000000000000, 0.000000000000000000 ) ) ;
#38179=VERTEX_POINT ( 'NONE', #58201 ) ;
#38181=VERTEX_POINT ( 'NONE', #42489 ) ;
#38182=VECTOR ( 'NONE', #85800, 1000.000000000000114 ) ;
#38183=VERTEX_POINT ( 'NONE', #88648 ) ;
#38184=FACE_OUTER_BOUND ( 'NONE', #54569, .T. ) ;
#38185=CARTESIAN_POINT ( 'NONE',  ( -74.58953762381672448, -24.66019654487198665, 8.947790411086131712 ) ) ;
#38186=CARTESIAN_POINT ( 'NONE',  ( -77.62287095715007013, -24.65952944569304606, 1.056160979905699016 ) ) ;
#38187=CARTESIAN_POINT ( 'NONE',  ( -20.51892249978613236, 2.527598752449112585, -1.500000000000002220 ) ) ;
#38189=CARTESIAN_POINT ( 'NONE',  ( 14.26105141482337935, -16.23293960606763520, 11.49999999999999645 ) ) ;
#38190=ORIENTED_EDGE ( 'NONE', *, *, #8865, .F. ) ;
#38192=CARTESIAN_POINT ( 'NONE',  ( -81.62287095715004170, -24.66019654487199020, 8.947790411086131712 ) ) ;
#38193=CARTESIAN_POINT ( 'NONE',  ( -60.62287095715005592, -23.84047902841601285, -0.8780736468305713194 ) ) ;
#38194=CARTESIAN_POINT ( 'NONE',  ( -15.72835732567950195, 15.92727474065614501, 11.49999999999998934 ) ) ;
#38195=AXIS2_PLACEMENT_3D ( 'NONE', #56328, #79633, #17237 ) ;
#38196=ADVANCED_FACE ( 'NONE', ( #50579 ), #73912, .T. ) ;
#38197=CARTESIAN_POINT ( 'NONE',  ( -62.52287095715006160, -23.96127896941631974, -0.6493128931038026908 ) ) ;
#38199=ORIENTED_EDGE ( 'NONE', *, *, #77398, .F. ) ;
#38201=CARTESIAN_POINT ( 'NONE',  ( -35.46595863577746854, -25.00182538069146077, 7.747789668545035369 ) ) ;
#38202=EDGE_CURVE ( 'NONE', #47437, #45447, #64354, .T. ) ;
#38204=CARTESIAN_POINT ( 'NONE',  ( -18.75169668496848985, 9.291489096422434812, -1.500000000000002220 ) ) ;
#38205=ADVANCED_FACE ( 'NONE', ( #28235 ), #84011, .T. ) ;
#38207=CARTESIAN_POINT ( 'NONE',  ( -67.54034052825554113, -24.51419770103159124, 9.386484678747168076 ) ) ;
#38208=ORIENTED_EDGE ( 'NONE', *, *, #59194, .T. ) ;
#38209=ORIENTED_EDGE ( 'NONE', *, *, #74673, .F. ) ;
#38211=CARTESIAN_POINT ( 'NONE',  ( 15.93590435955092843, -13.91358336426615239, -1.500000000000002220 ) ) ;
#38212=VERTEX_POINT ( 'NONE', #95895 ) ;
#38213=CARTESIAN_POINT ( 'NONE',  ( -112.5228709571500332, -24.33927499327855770, 9.819080762295804732 ) ) ;
#38214=CARTESIAN_POINT ( 'NONE',  ( -99.37409858214790859, -25.12215546412569012, 6.508817117250577766 ) ) ;
#38215=CARTESIAN_POINT ( 'NONE',  ( -12.70408864715453667, 17.69581422525067183, 11.49999999999998934 ) ) ;
#38216=CARTESIAN_POINT ( 'NONE',  ( -89.23534077628077910, -25.22391154813774605, 6.409327647370973935 ) ) ;
#38217=CARTESIAN_POINT ( 'NONE',  ( -76.60618700539868087, -23.48786465467240703, 11.44779295918254647 ) ) ;
#38219=CARTESIAN_POINT ( 'NONE',  ( 3.468383421097696928, -21.53508805063734854, -1.500000000000002220 ) ) ;
#38220=CARTESIAN_POINT ( 'NONE',  ( -71.70841769935768184, -25.31639753719101549, 6.192981292503872304 ) ) ;
#38221=ORIENTED_EDGE ( 'NONE', *, *, #83815, .F. ) ;
#38223=DIRECTION ( 'NONE',  ( 1.000000000000000000, 3.773278334444165844E-23, 8.201307836089272790E-29 ) ) ;
#38224=CARTESIAN_POINT ( 'NONE',  ( -72.55620429048340725, -24.65952944569304606, 1.056160979905698127 ) ) ;
#38225=CARTESIAN_POINT ( 'NONE',  ( -43.62287095715004881, -23.47593901973091235, -1.443836447539011525 ) ) ;
#38226=ORIENTED_EDGE ( 'NONE', *, *, #42824, .T. ) ;
#38227=B_SPLINE_CURVE_WITH_KNOTS ( 'NONE', 3,
 ( #3294, #89503, #19987, #57076 ),
 .UNSPECIFIED., .F., .F.,
 ( 4, 4 ),
 ( 0.000000000000000000, 0.0009166666666666628549 ),
 .UNSPECIFIED. ) ;
#38229=ORIENTED_EDGE ( 'NONE', *, *, #65772, .T. ) ;
#38231=CARTESIAN_POINT ( 'NONE',  ( 16.91677535067316995, -12.78530099663392505, 11.49999999999998934 ) ) ;
#38232=CARTESIAN_POINT ( 'NONE',  ( -94.62287095715007013, -23.73907113216990794, -1.053371485793227702 ) ) ;
#38233=CARTESIAN_POINT ( 'NONE',  ( -30.63234162661936111, -23.86952536761623023, -1.017619990082605952 ) ) ;
#38234=CARTESIAN_POINT ( 'NONE',  ( -99.55620429048339304, -24.64898659630529210, 1.056161002820829919 ) ) ;
#38236=CARTESIAN_POINT ( 'NONE',  ( -11.15089393765527959, -15.82809448842462885, 11.49999999999998934 ) ) ;
#38237=CARTESIAN_POINT ( 'NONE',  ( -39.02569778787134425, -25.30060000302003331, 6.009290021095885059 ) ) ;
#38238=ORIENTED_EDGE ( 'NONE', *, *, #54819, .T. ) ;
#38239=CARTESIAN_POINT ( 'NONE',  ( -18.83898130102433299, -4.906684326670742280, 11.49999999999999645 ) ) ;
#38240=DIRECTION ( 'NONE',  ( -1.000000000000000000, -3.773278334444166432E-23, -8.201307841325785021E-29 ) ) ;
#38241=CARTESIAN_POINT ( 'NONE',  ( -103.5228709571500900, -24.33927499327855415, 9.819080762295806508 ) ) ;
#38242=ORIENTED_EDGE ( 'NONE', *, *, #66341, .F. ) ;
#38243=DIRECTION ( 'NONE',  ( -0.000000000000000000, 2.173523156925979552E-06, -0.9999999999976378895 ) ) ;
#38245=VECTOR ( 'NONE', #31973, 1000.000000000000114 ) ;
#38246=PLANE ( 'NONE',  #6643 ) ;
#38247=EDGE_CURVE ( 'NONE', #5695, #39942, #57361, .T. ) ;
#38248=CARTESIAN_POINT ( 'NONE',  ( -55.62287095715002749, -24.92579138211018375, 1.929029949965663349 ) ) ;
#38249=CARTESIAN_POINT ( 'NONE',  ( 19.40334540789412188, 3.064012487144803565, 11.49999999999998934 ) ) ;
#38250=CARTESIAN_POINT ( 'NONE',  ( -40.99816688406356491, -25.31583739607578920, 4.936760826533250324 ) ) ;
#38251=VERTEX_POINT ( 'NONE', #81171 ) ;
#38252=CARTESIAN_POINT ( 'NONE',  ( -2.376235263977734657, 21.45616117177731041, -1.500000000000002220 ) ) ;
#38254=CARTESIAN_POINT ( 'NONE',  ( -40.63664402775552986, -24.63355581998383670, 0.9682620441943914358 ) ) ;
#38256=CARTESIAN_POINT ( 'NONE',  ( 11.60186680256600233, 19.91347440808847935, -1.500000000000002220 ) ) ;
#38257=EDGE_CURVE ( 'NONE', #23443, #11463, #81675, .T. ) ;
#38258=AXIS2_PLACEMENT_3D ( 'NONE', #23056, #92086, #99193 ) ;
#38260=CARTESIAN_POINT ( 'NONE',  ( -93.56158353983492759, -23.48783264082477018, -1.443836473390090358 ) ) ;
#38262=CARTESIAN_POINT ( 'NONE',  ( -18.82339984186270598, 7.397194320553815317, 11.49999999999999645 ) ) ;
#38263=DIRECTION ( 'NONE',  ( -3.773278334453079618E-23, 0.9999999999976377785, 2.173523156925978705E-06 ) ) ;
#38265=AXIS2_PLACEMENT_3D ( 'NONE', #89630, #26234, #20111 ) ;
#38266=CARTESIAN_POINT ( 'NONE',  ( -110.3641915914744800, -25.29823811401694655, 2.833513268873118829 ) ) ;
#38267=CARTESIAN_POINT ( 'NONE',  ( -34.62287095715005592, -29.50250786944525672, 11.44777988621624409 ) ) ;
#38268=CARTESIAN_POINT ( 'NONE',  ( -122.5228709571500332, -24.51387760970725438, 9.387446482453409402 ) ) ;
#38269=CARTESIAN_POINT ( 'NONE',  ( 12.47747183659840786, 15.48776231947736015, 11.49999999999998934 ) ) ;
#38270=VECTOR ( 'NONE', #10303, 1000.000000000000114 ) ;
#38271=PLANE ( 'NONE',  #79237 ) ;
#38272=CARTESIAN_POINT ( 'NONE',  ( -15.09475962229707591, 12.77647934908296712, -1.500000000000002220 ) ) ;
#38273=AXIS2_PLACEMENT_3D ( 'NONE', #96216, #34813, #43433 ) ;
#38274=CARTESIAN_POINT ( 'NONE',  ( -56.54233644916853763, -24.34968618360933590, 0.1864209137778786995 ) ) ;
#38275=FACE_OUTER_BOUND ( 'NONE', #46748, .T. ) ;
#38277=CARTESIAN_POINT ( 'NONE',  ( -13.38394104848841693, -15.81244124602197765, 11.49999999999999645 ) ) ;
#38278=CARTESIAN_POINT ( 'NONE',  ( -38.52287095715006870, -29.50248528299804818, 1.056150453629031594 ) ) ;
#38280=CARTESIAN_POINT ( 'NONE',  ( -35.52287095715006870, -23.47596703998600631, 11.44779298504229281 ) ) ;
#38281=B_SPLINE_CURVE_WITH_KNOTS ( 'NONE', 3,
 ( #47469, #78396, #8899, #39845, #94632, #32230, #63204, #2302 ),
 .UNSPECIFIED., .F., .F.,
 ( 4, 2, 2, 4 ),
 ( 0.000000000000000000, 0.002001079623178220190, 0.003001619434767332020, 0.004002159246356443850 ),
 .UNSPECIFIED. ) ;
#38282=CARTESIAN_POINT ( 'NONE',  ( -5.793434319722853054, -21.96748078227757617, 11.49999999999999645 ) ) ;
#38286=CARTESIAN_POINT ( 'NONE',  ( -15.75104486599040321, 12.61009050114280861, -1.500000000000002220 ) ) ;
#38287=B_SPLINE_CURVE_WITH_KNOTS ( 'NONE', 3,
 ( #584, #17311, #25928, #93931 ),
 .UNSPECIFIED., .F., .F.,
 ( 4, 4 ),
 ( 0.000000000000000000, 9.999999999998897304E-05 ),
 .UNSPECIFIED. ) ;
#38289=DIRECTION ( 'NONE',  ( -3.773278334453079618E-23, 0.9999999999976377785, 2.173523156925979975E-06 ) ) ;
#38290=EDGE_CURVE ( 'NONE', #85635, #76224, #11160, .T. ) ;
#38294=FACE_OUTER_BOUND ( 'NONE', #12011, .T. ) ;
#38295=CARTESIAN_POINT ( 'NONE',  ( 18.56524475492553705, -13.42312393814442650, 11.49999999999998934 ) ) ;
#38297=CARTESIAN_POINT ( 'NONE',  ( -21.01067979154616694, 5.129389437380057259, -1.500000000000002220 ) ) ;
#38298=CARTESIAN_POINT ( 'NONE',  ( -123.5209524854786167, -23.96119346886881019, -0.6495511937832023630 ) ) ;
#38300=CARTESIAN_POINT ( 'NONE',  ( -0.8937202392249329330, 20.86669477224961256, 11.49999999999999645 ) ) ;
#38302=CARTESIAN_POINT ( 'NONE',  ( -68.99199226862026535, -25.31612623828177888, 5.787353048591010740 ) ) ;
#38303=CARTESIAN_POINT ( 'NONE',  ( -2.093881351098874521, -21.91542971883435698, -1.500000000000002220 ) ) ;
#38304=CARTESIAN_POINT ( 'NONE',  ( -64.52287095715006160, -23.47593901973090169, -1.443836447538996870 ) ) ;
#38305=CARTESIAN_POINT ( 'NONE',  ( -27.89469851781394283, -24.79700315216039996, 7.595246444988488221 ) ) ;
#38309=EDGE_LOOP ( 'NONE', ( #1286, #34909, #80987, #75646 ) ) ;
#38311=ORIENTED_EDGE ( 'NONE', *, *, #31197, .F. ) ;
#38313=ADVANCED_FACE ( 'NONE', ( #11651 ), #67817, .T. ) ;
#38314=CARTESIAN_POINT ( 'NONE',  ( -61.64687923781919920, -25.13069339737145214, 2.947789366383932297 ) ) ;
#38315=CARTESIAN_POINT ( 'NONE',  ( -95.62287095714998486, -23.85229601348997264, 10.88205029486207032 ) ) ;
#38316=CARTESIAN_POINT ( 'NONE',  ( -100.5228709571500758, -24.91570333825770689, 8.075032458260348989 ) ) ;
#38317=CARTESIAN_POINT ( 'NONE',  ( 10.21088607376515789, 17.76353854702842483, -1.500000000000002220 ) ) ;
#38318=ORIENTED_EDGE ( 'NONE', *, *, #63259, .T. ) ;
#38322=CARTESIAN_POINT ( 'NONE',  ( 13.76814385225720372, 17.53657229028232223, -1.500000000000002220 ) ) ;
#38324=B_SPLINE_CURVE_WITH_KNOTS ( 'NONE', 3,
 ( #48791, #4104, #18323, #27442 ),
 .UNSPECIFIED., .F., .F.,
 ( 4, 4 ),
 ( 6.938893903907228378E-18, 9.999999999999591193E-05 ),
 .UNSPECIFIED. ) ;
#38325=B_SPLINE_CURVE_WITH_KNOTS ( 'NONE', 3,
 ( #41382, #72838, #20034, #58602 ),
 .UNSPECIFIED., .F., .F.,
 ( 4, 4 ),
 ( 0.1398858135129756319, 0.1488922447850913322 ),
 .UNSPECIFIED. ) ;
#38328=ORIENTED_EDGE ( 'NONE', *, *, #40380, .F. ) ;
#38329=CARTESIAN_POINT ( 'NONE',  ( -29.59050140619070746, -25.08417512812387784, 3.123287764124576427 ) ) ;
#38330=CARTESIAN_POINT ( 'NONE',  ( -39.52287095715006160, -23.96177878511308634, 10.65340807706330573 ) ) ;
#38331=ADVANCED_FACE ( 'NONE', ( #3560 ), #65478, .F. ) ;
#38332=CARTESIAN_POINT ( 'NONE',  ( -20.21371806590929410, -4.994250807877889109, 11.49999999999998934 ) ) ;
#38333=EDGE_CURVE ( 'NONE', #75143, #79503, #26887, .T. ) ;
#38334=VERTEX_POINT ( 'NONE', #2562 ) ;
#38335=CARTESIAN_POINT ( 'NONE',  ( -42.52287095715006870, -24.51387760970724372, 9.387446482453423613 ) ) ;
#38338=CARTESIAN_POINT ( 'NONE',  ( -98.52287095715009002, -24.66019654487200441, 8.947790411086119278 ) ) ;
#38339=VERTEX_POINT ( 'NONE', #33498 ) ;
#38340=VERTEX_POINT ( 'NONE', #64484 ) ;
#38341=VECTOR ( 'NONE', #85372, 1000.000000000000114 ) ;
#38342=DIRECTION ( 'NONE',  ( 1.000000000000000000, 3.773278334444167608E-23, 8.201307833595939069E-29 ) ) ;
#38343=CARTESIAN_POINT ( 'NONE',  ( -80.58953762381672448, -24.99156044556120193, 7.747789690856343725 ) ) ;
#38344=CARTESIAN_POINT ( 'NONE',  ( -110.7941337500641765, -25.27168412048538571, 6.209429327144849076 ) ) ;
#38346=CARTESIAN_POINT ( 'NONE',  ( -99.12380231474227799, -25.26431306044052150, 4.001575155705512366 ) ) ;
#38347=CARTESIAN_POINT ( 'NONE',  ( -92.50696408965231399, -24.51419770103157347, 9.386484678747171628 ) ) ;
#38349=CARTESIAN_POINT ( 'NONE',  ( -21.51168160490077952, -5.175097382202364926, 11.49999999999999645 ) ) ;
#38350=VERTEX_POINT ( 'NONE', #75537 ) ;
#38351=ADVANCED_FACE ( 'NONE', ( #59846 ), #60847, .T. ) ;
#38352=DIRECTION ( 'NONE',  ( -1.000000000000000000, -3.773278334444167608E-23, -8.201307833595939069E-29 ) ) ;
#38354=CARTESIAN_POINT ( 'NONE',  ( 22.31954755298990278, 3.869410565987296380, -1.500000000000002220 ) ) ;
#38355=VECTOR ( 'NONE', #28302, 1000.000000000000114 ) ;
#38356=CARTESIAN_POINT ( 'NONE',  ( -29.10259911666015498, -25.11412234476797067, 6.379066241192269615 ) ) ;
#38358=ORIENTED_EDGE ( 'NONE', *, *, #84868, .T. ) ;
#38359=CARTESIAN_POINT ( 'NONE',  ( -99.58953762381672448, -24.65952944569304606, 1.056160979905699682 ) ) ;
#38360=CARTESIAN_POINT ( 'NONE',  ( -19.81368827760683260, -3.497637702615509880, 11.49999999999998934 ) ) ;
#38363=B_SPLINE_CURVE_WITH_KNOTS ( 'NONE', 3,
 ( #60902, #60408, #82717, #5599 ),
 .UNSPECIFIED., .F., .F.,
 ( 4, 4 ),
 ( 0.7503217108452443496, 0.7593281421173597723 ),
 .UNSPECIFIED. ) ;
#38364=CARTESIAN_POINT ( 'NONE',  ( -92.62287095715005592, -23.48786465467241413, 11.44779295918254469 ) ) ;
#38365=CARTESIAN_POINT ( 'NONE',  ( -21.16112330106665240, 7.131417522999676351, -1.500000000000002220 ) ) ;
#38366=EDGE_LOOP ( 'NONE', ( #4758, #85247, #59046, #64663 ) ) ;
#38367=ORIENTED_EDGE ( 'NONE', *, *, #22103, .F. ) ;
#38371=VECTOR ( 'NONE', #27613, 1000.000000000000114 ) ;
#38372=FACE_OUTER_BOUND ( 'NONE', #55539, .T. ) ;
#38374=CARTESIAN_POINT ( 'NONE',  ( 17.37147561666312257, 8.948746033654231269, -1.500000000000002220 ) ) ;
#38376=CARTESIAN_POINT ( 'NONE',  ( 10.45947017991876926, -18.73710855793504848, 11.49999999999998934 ) ) ;
#38379=FACE_OUTER_BOUND ( 'NONE', #69893, .T. ) ;
#38380=CARTESIAN_POINT ( 'NONE',  ( -129.5228709571500758, -23.48786465467242479, 11.44779295918253581 ) ) ;
#38382=CARTESIAN_POINT ( 'NONE',  ( 6.305670413343573699, 22.00876638805999974, -1.500000000000002220 ) ) ;
#38385=CARTESIAN_POINT ( 'NONE',  ( -101.5895376238167245, -23.47593901973091235, -1.443836447539001089 ) ) ;
#38387=CARTESIAN_POINT ( 'NONE',  ( -0.1815635828756200498, -20.05798930676971636, 11.49999999999999645 ) ) ;
#38388=CARTESIAN_POINT ( 'NONE',  ( -79.67189865184847974, -25.26612408227589768, 4.664461613298229281 ) ) ;
#38392=ORIENTED_EDGE ( 'NONE', *, *, #47136, .F. ) ;
#38393=CARTESIAN_POINT ( 'NONE',  ( -109.5228709571500332, -23.94994826722564696, -0.6494450866342718065 ) ) ;
#38395=CARTESIAN_POINT ( 'NONE',  ( -12.78816955685674372, 17.57309652720472570, 11.49999999999998934 ) ) ;
#38396=CARTESIAN_POINT ( 'NONE',  ( -39.62287095715005592, -29.50250243563736774, 8.947779886222148704 ) ) ;
#38397=CARTESIAN_POINT ( 'NONE',  ( -12.94911239430987315, -14.73082512860577609, -1.500000000000002220 ) ) ;
#38398=AXIS2_PLACEMENT_3D ( 'NONE', #27397, #94897, #11657 ) ;
#38400=B_SPLINE_CURVE_WITH_KNOTS ( 'NONE', 3,
 ( #3257, #17453, #10851, #33180, #96090, #87978 ),
 .UNSPECIFIED., .F., .F.,
 ( 4, 2, 4 ),
 ( 6.391158118973930141E-06, 0.001387004593080793519, 0.002767618028042612838 ),
 .UNSPECIFIED. ) ;
#38401=CARTESIAN_POINT ( 'NONE',  ( -109.4462232385598099, -25.27925759040196141, 4.635298292504290707 ) ) ;
#38403=PLANE ( 'NONE',  #90466 ) ;
#38405=CARTESIAN_POINT ( 'NONE',  ( -18.14515864413662172, 9.488524743509296755, 11.49999999999999645 ) ) ;
#38406=DIRECTION ( 'NONE',  ( -3.773278334453079030E-23, 0.9999999999976377785, 2.173523156925979128E-06 ) ) ;
#38408=CARTESIAN_POINT ( 'NONE',  ( -120.5169643464197975, -24.83618233451451118, 1.606449574219542598 ) ) ;
#38409=EDGE_CURVE ( 'NONE', #26640, #51831, #6546, .T. ) ;
#38410=ORIENTED_EDGE ( 'NONE', *, *, #70788, .T. ) ;
#38411=CARTESIAN_POINT ( 'NONE',  ( -99.65355524409876864, -25.31296369576671523, 4.362766217231969890 ) ) ;
#38413=CARTESIAN_POINT ( 'NONE',  ( -125.6251146265216221, -24.15602025860897584, 10.28564288303534013 ) ) ;
#38417=CARTESIAN_POINT ( 'NONE',  ( -25.53444008324515124, -24.61459456346077701, 5.226875869559658661 ) ) ;
#38421=CARTESIAN_POINT ( 'NONE',  ( 22.66633601775066253, -4.223608244049824378, 11.49999999999999645 ) ) ;
#38422=CARTESIAN_POINT ( 'NONE',  ( 21.14626179850551324, 8.528272852130310611, 11.49999999999998934 ) ) ;
#38423=CARTESIAN_POINT ( 'NONE',  ( -74.64912136475619775, -23.48783264082477018, -1.443836473390096353 ) ) ;
#38424=CARTESIAN_POINT ( 'NONE',  ( -96.63903541359736948, -23.48783264082477018, -1.443836473390089914 ) ) ;
#38427=CARTESIAN_POINT ( 'NONE',  ( -20.38924965233672282, -9.335317855073830273, 11.49999999999999645 ) ) ;
#38428=ORIENTED_EDGE ( 'NONE', *, *, #18417, .F. ) ;
#38429=CARTESIAN_POINT ( 'NONE',  ( -40.52287095715007581, -25.00182538069145011, 7.747789668545104647 ) ) ;
#38430=PLANE ( 'NONE',  #22169 ) ;
#38431=CARTESIAN_POINT ( 'NONE',  ( -21.18249553426131015, -5.656070447573528170, 11.49999999999998934 ) ) ;
#38434=CARTESIAN_POINT ( 'NONE',  ( -77.62287095715007013, -24.65952944569304606, 1.056160979905699016 ) ) ;
#38435=CARTESIAN_POINT ( 'NONE',  ( -125.5228709571500616, -24.99156044556120904, 7.747789690856173195 ) ) ;
#38437=VERTEX_POINT ( 'NONE', #68445 ) ;
#38438=CARTESIAN_POINT ( 'NONE',  ( -4.979992623568794130, 19.86841884474198494, 11.49999999999998934 ) ) ;
#38440=ORIENTED_EDGE ( 'NONE', *, *, #74230, .F. ) ;
#38441=ORIENTED_EDGE ( 'NONE', *, *, #62971, .T. ) ;
#38442=ORIENTED_EDGE ( 'NONE', *, *, #46272, .T. ) ;
#38443=EDGE_CURVE ( 'NONE', #4897, #24545, #67957, .T. ) ;
#38444=CARTESIAN_POINT ( 'NONE',  ( -23.06710473063640165, 0.7821689226722955413, -1.500000000000002220 ) ) ;
#38445=CARTESIAN_POINT ( 'NONE',  ( -102.5228709571501042, -24.66019654487200441, 8.947790411086119278 ) ) ;
#38446=CARTESIAN_POINT ( 'NONE',  ( 17.43904876784772284, 10.37648870149486413, -1.500000000000002220 ) ) ;
#38447=ORIENTED_EDGE ( 'NONE', *, *, #33885, .T. ) ;
#38451=CARTESIAN_POINT ( 'NONE',  ( -73.52287095715007581, -24.64965694238407323, 8.947790433994200043 ) ) ;
#38452=CARTESIAN_POINT ( 'NONE',  ( -70.63767667287973495, -24.40034930558990922, 0.3402023900116040167 ) ) ;
#38453=CARTESIAN_POINT ( 'NONE',  ( -10.41973078503355588, 18.78793304046337198, 11.49999999999999645 ) ) ;
#38454=VERTEX_POINT ( 'NONE', #60352 ) ;
#38455=CARTESIAN_POINT ( 'NONE',  ( -125.6228709571500559, -24.99132157543083821, 2.256160258750667502 ) ) ;
#38456=CARTESIAN_POINT ( 'NONE',  ( -34.62287095715005592, -24.64898659630367206, 1.056161002820817485 ) ) ;
#38458=AXIS2_PLACEMENT_3D ( 'NONE', #23505, #22009, #7801 ) ;
#38459=CARTESIAN_POINT ( 'NONE',  ( -17.53982812869053731, -11.02811673548155902, 11.49999999999998934 ) ) ;
#38462=CARTESIAN_POINT ( 'NONE',  ( -123.6228709571500559, -23.48783264082478794, -1.443836473390058606 ) ) ;
#38464=B_SPLINE_SURFACE_WITH_KNOTS ( 'NONE', 3, 3, ( 
 ( #67680, #98600, #76256, #61059 ),
 ( #52444, #6751, #6256, #36220 ),
 ( #12863, #67183, #13864, #37705 ),
 ( #68665, #91989, #90993, #51945 ),
 ( #22460, #84376, #76744, #21464 ),
 ( #69154, #86383, #69664, #39700 ),
 ( #32593, #9757, #16866, #63064 ) ),
 .UNSPECIFIED., .F., .F., .F.,
 ( 4, 3, 4 ),
 ( 4, 4 ),
 ( 0.0004766839783816787229, 0.1029713700210895116, 0.2054660560637973366 ),
 ( 0.4596109144125399837, 0.4608357025999801904 ),
 .UNSPECIFIED. ) ;
#38467=ORIENTED_EDGE ( 'NONE', *, *, #23539, .F. ) ;
#38469=CARTESIAN_POINT ( 'NONE',  ( -55.52287095715007581, -23.84081130425355610, 10.88220057483161085 ) ) ;
#38470=CARTESIAN_POINT ( 'NONE',  ( -77.62287095715009855, -23.47596703998600631, 11.44779298504227683 ) ) ;
#38471=CARTESIAN_POINT ( 'NONE',  ( -65.49304012721087531, -24.63355581998386867, 0.9682620441943842193 ) ) ;
#38472=CARTESIAN_POINT ( 'NONE',  ( -4.682628417673765142, 21.48327871026360114, 11.49999999999999645 ) ) ;
#38473=EDGE_CURVE ( 'NONE', #85527, #32572, #70446, .T. ) ;
#38474=CARTESIAN_POINT ( 'NONE',  ( -89.54841333971366168, -24.35071581493543391, 9.817618358456025263 ) ) ;
#38475=CARTESIAN_POINT ( 'NONE',  ( -5.352388609804938469, -21.92410630658433845, -1.500000000000002220 ) ) ;
#38476=VECTOR ( 'NONE', #64506, 1000.000000000000114 ) ;
#38477=CARTESIAN_POINT ( 'NONE',  ( -12.59924929152775874, 16.77720732749412846, -1.500000000000002220 ) ) ;
#38478=EDGE_CURVE ( 'NONE', #84725, #15126, #93419, .T. ) ;
#38479=PLANE ( 'NONE',  #70723 ) ;
#38480=DIRECTION ( 'NONE',  ( -1.000000000000000000, -3.773278334444167608E-23, -8.201307833595939069E-29 ) ) ;
#38482=EDGE_CURVE ( 'NONE', #96355, #31349, #11128, .T. ) ;
#38483=EDGE_LOOP ( 'NONE', ( #2932, #28331, #72317, #49732 ) ) ;
#38487=CARTESIAN_POINT ( 'NONE',  ( 4.199879391047538491, -21.09745483596041282, -1.500000000000002220 ) ) ;
#38490=CARTESIAN_POINT ( 'NONE',  ( -4.502559807402421121, -20.62786074129878955, -1.500000000000002220 ) ) ;
#38491=CARTESIAN_POINT ( 'NONE',  ( -47.52287095715006160, -29.50250243563736774, 8.947779886222146928 ) ) ;
#38492=CARTESIAN_POINT ( 'NONE',  ( -59.79580795642156232, -25.14083923594471059, 2.947789366366678987 ) ) ;
#38493=CARTESIAN_POINT ( 'NONE',  ( -83.59183038314901637, -24.15620529776628089, 10.23563542870660470 ) ) ;
#38494=VECTOR ( 'NONE', #85155, 1000.000000000000114 ) ;
#38495=CARTESIAN_POINT ( 'NONE',  ( -56.62287095715004881, -24.66019654487199020, 8.947790411086131712 ) ) ;
#38496=CARTESIAN_POINT ( 'NONE',  ( -127.5228709571500332, -24.66019654487200441, 8.947790411086105067 ) ) ;
#38497=CARTESIAN_POINT ( 'NONE',  ( 18.07010470096111021, 12.80550835427630574, -1.500000000000002220 ) ) ;
#38498=CARTESIAN_POINT ( 'NONE',  ( -81.64592523690049575, -23.48786465467241413, 11.44779295918254824 ) ) ;
#38499=ORIENTED_EDGE ( 'NONE', *, *, #12986, .F. ) ;
#38501=CARTESIAN_POINT ( 'NONE',  ( -64.52287095715006160, -23.47593901973090169, -1.443836447538996870 ) ) ;
#38502=CARTESIAN_POINT ( 'NONE',  ( -68.62287095715005592, -24.64898659630367916, 1.056161002820824368 ) ) ;
#38503=CARTESIAN_POINT ( 'NONE',  ( -100.6235771224457665, -25.00158670708910691, 2.256160236439218369 ) ) ;
#38504=CARTESIAN_POINT ( 'NONE',  ( 17.17441491540288823, 9.109037055621362455, 11.49999999999998934 ) ) ;
#38505=CARTESIAN_POINT ( 'NONE',  ( -20.23222619987061677, -6.887663580918623296, 11.49999999999998934 ) ) ;
#38508=CARTESIAN_POINT ( 'NONE',  ( -111.9545715455114987, -25.05712135967895193, 7.447789548357302891 ) ) ;
#38510=CARTESIAN_POINT ( 'NONE',  ( 19.36006514395606004, 11.85157241509795512, -1.500000000000002220 ) ) ;
#38511=CARTESIAN_POINT ( 'NONE',  ( -106.5895376238167387, -23.47593901973091235, -1.443836447538999312 ) ) ;
#38513=CARTESIAN_POINT ( 'NONE',  ( -19.69265041987409859, 1.759638296948408787, 11.49999999999999645 ) ) ;
#38514=CARTESIAN_POINT ( 'NONE',  ( -88.58953762381669605, -24.64898659630367916, 1.056161002820386052 ) ) ;
#38515=VERTEX_POINT ( 'NONE', #30374 ) ;
#38517=CARTESIAN_POINT ( 'NONE',  ( -99.29687923781919778, -25.26138073939643292, 6.149712181314777482 ) ) ;
#38519=CARTESIAN_POINT ( 'NONE',  ( 15.40532884848888884, -15.22192433072940609, -1.500000000000002220 ) ) ;
#38522=CARTESIAN_POINT ( 'NONE',  ( 14.64286990871793392, 12.78475832571431070, -1.500000000000002220 ) ) ;
#38523=CARTESIAN_POINT ( 'NONE',  ( -80.52287095715004739, -25.00182538069145366, 7.747789668545104647 ) ) ;
#38524=CARTESIAN_POINT ( 'NONE',  ( -55.49173473690001401, -24.52399227489126687, 9.353111116836526406 ) ) ;
#38525=CARTESIAN_POINT ( 'NONE',  ( 15.56394622224390645, 12.30447529683395125, 11.49999999999998934 ) ) ;
#38526=VERTEX_POINT ( 'NONE', #38495 ) ;
#38527=CARTESIAN_POINT ( 'NONE',  ( -8.236308187080631171, 18.58821751820538637, 11.49999999999999645 ) ) ;
#38528=CARTESIAN_POINT ( 'NONE',  ( -80.49584335415009662, -24.83618233451450408, 1.606449574219532384 ) ) ;
#38530=EDGE_CURVE ( 'NONE', #6142, #44485, #933, .T. ) ;
#38532=CARTESIAN_POINT ( 'NONE',  ( -30.61048516611183601, -24.43626637953622449, 0.1835287498755956703 ) ) ;
#38533=CARTESIAN_POINT ( 'NONE',  ( -92.52287095715006160, -24.64898659630529210, 1.056161002820827921 ) ) ;
#38534=CARTESIAN_POINT ( 'NONE',  ( -49.13746579462012676, -25.31601915193193975, 5.391919824163067254 ) ) ;
#38536=DIRECTION ( 'NONE',  ( 0.000000000000000000, 2.173523156925980399E-06, -0.9999999999976378895 ) ) ;
#38537=CARTESIAN_POINT ( 'NONE',  ( 10.01938154005162218, -17.43019892170380913, -1.500000000000002220 ) ) ;
#38538=CARTESIAN_POINT ( 'NONE',  ( -122.6228709571500417, -29.50247984919015209, -1.443849546365046699 ) ) ;
#38540=EDGE_CURVE ( 'NONE', #69591, #31747, #23755, .T. ) ;
#38543=AXIS2_PLACEMENT_3D ( 'NONE', #58736, #43519, #89685 ) ;
#38545=CARTESIAN_POINT ( 'NONE',  ( -8.048360580058307789, -21.46040670285860230, 11.49999999999999645 ) ) ;
#38546=CARTESIAN_POINT ( 'NONE',  ( -22.42851769774927817, -3.676000928666301792, -1.500000000000002220 ) ) ;
#38547=ORIENTED_EDGE ( 'NONE', *, *, #84916, .T. ) ;
#38548=CARTESIAN_POINT ( 'NONE',  ( -109.6228709571500701, -24.34917612406837861, 0.1852690917426676465 ) ) ;
#38549=CARTESIAN_POINT ( 'NONE',  ( -126.5228709571500616, -23.48786465467241769, 11.44779295918253581 ) ) ;
#38550=CARTESIAN_POINT ( 'NONE',  ( -39.50187459890584307, -25.26395632038229522, 3.881371279102487026 ) ) ;
#38552=CARTESIAN_POINT ( 'NONE',  ( -30.57287095715007297, -25.31541627316749654, 4.725453788811557310 ) ) ;
#38554=CARTESIAN_POINT ( 'NONE',  ( -128.5217320095746061, -24.15620529776629510, 10.23563542870659582 ) ) ;
#38555=FACE_OUTER_BOUND ( 'NONE', #91973, .T. ) ;
#38556=ORIENTED_EDGE ( 'NONE', *, *, #45111, .T. ) ;
#38558=CARTESIAN_POINT ( 'NONE',  ( 12.54693703879240196, 16.07252283493236433, -1.500000000000002220 ) ) ;
#38559=B_SPLINE_CURVE_WITH_KNOTS ( 'NONE', 3,
 ( #25075, #55550, #38803, #85985 ),
 .UNSPECIFIED., .F., .F.,
 ( 4, 4 ),
 ( 0.7102931274136203843, 0.7192995586857354740 ),
 .UNSPECIFIED. ) ;
#38561=ADVANCED_FACE ( 'NONE', ( #92270 ), #16646, .T. ) ;
#38562=CARTESIAN_POINT ( 'NONE',  ( 16.94363762160741516, 15.55198921429254533, -1.500000000000002220 ) ) ;
#38563=CARTESIAN_POINT ( 'NONE',  ( -45.52287095715006160, -24.99132157543083821, 2.256160258750667502 ) ) ;
#38564=VERTEX_POINT ( 'NONE', #31377 ) ;
#38565=CARTESIAN_POINT ( 'NONE',  ( -101.1944152955115044, -25.16311295231453826, 6.858246048749960799 ) ) ;
#38567=EDGE_CURVE ( 'NONE', #55380, #73391, #9039, .T. ) ;
#38568=CARTESIAN_POINT ( 'NONE',  ( -51.62815728054503239, -24.51419770103156637, 9.386484678747176957 ) ) ;
#38569=CARTESIAN_POINT ( 'NONE',  ( 19.98919582620916913, -7.218065965386815996, 11.49999999999999645 ) ) ;
#38570=ORIENTED_EDGE ( 'NONE', *, *, #83784, .T. ) ;
#38571=EDGE_LOOP ( 'NONE', ( #39185, #88130, #33241, #1243 ) ) ;
#38572=CARTESIAN_POINT ( 'NONE',  ( 20.56832688555235222, -8.368550285707721414, -1.500000000000002220 ) ) ;
#38573=CARTESIAN_POINT ( 'NONE',  ( -7.709890279958820258, -19.11728055126480186, -1.500000000000002220 ) ) ;
#38574=ADVANCED_FACE ( 'NONE', ( #61844 ), #14648, .T. ) ;
#38576=EDGE_LOOP ( 'NONE', ( #32450, #92018, #87557, #79353 ) ) ;
#38577=CARTESIAN_POINT ( 'NONE',  ( -108.9979829822171951, -25.31627198676055457, 4.539662782732864166 ) ) ;
#38578=CARTESIAN_POINT ( 'NONE',  ( -39.32411912248426944, -25.20542183771704714, 3.367115814691465481 ) ) ;
#38580=CARTESIAN_POINT ( 'NONE',  ( -91.50657791617553016, -24.51314013834315375, 0.6176544820404143987 ) ) ;
#38582=CARTESIAN_POINT ( 'NONE',  ( -39.52287095715009002, -24.33927499327854349, 9.819080762295822495 ) ) ;
#38583=CARTESIAN_POINT ( 'NONE',  ( -48.52287095715007581, -23.47593901973090524, -1.443836447538997314 ) ) ;
#38584=CARTESIAN_POINT ( 'NONE',  ( -20.82185584224439978, -0.2524610531272265534, -1.500000000000002220 ) ) ;
#38585=CARTESIAN_POINT ( 'NONE',  ( 13.71991279636371175, 16.93377936151356877, 11.49999999999999645 ) ) ;
#38587=CARTESIAN_POINT ( 'NONE',  ( -78.50464208480038053, -24.35071581493543391, 9.817618358456027039 ) ) ;
#38588=CARTESIAN_POINT ( 'NONE',  ( -22.46026885398333661, -0.8929446408661095846, -1.500000000000002220 ) ) ;
#38589=EDGE_CURVE ( 'NONE', #70398, #29553, #92166, .T. ) ;
#38590=CARTESIAN_POINT ( 'NONE',  ( -50.38822539166533687, -25.26334751702766113, 4.736250638575107530 ) ) ;
#38591=ORIENTED_EDGE ( 'NONE', *, *, #14674, .T. ) ;
#38592=CARTESIAN_POINT ( 'NONE',  ( -58.52287095715006160, -23.73907113216989018, -1.053371485793251461 ) ) ;
#38593=DIRECTION ( 'NONE',  ( -3.773278334453079030E-23, 0.9999999999976377785, 2.173523156925979128E-06 ) ) ;
#38594=B_SPLINE_CURVE_WITH_KNOTS ( 'NONE', 3,
 ( #13305, #97556, #20415, #32789, #33285, #63772 ),
 .UNSPECIFIED., .F., .F.,
 ( 4, 2, 4 ),
 ( 0.000000000000000000, 0.001380764517854758894, 0.002761529035709517788 ),
 .UNSPECIFIED. ) ;
#38597=ORIENTED_EDGE ( 'NONE', *, *, #48419, .T. ) ;
#38598=EDGE_CURVE ( 'NONE', #43572, #31857, #54620, .T. ) ;
#38599=VERTEX_POINT ( 'NONE', #63355 ) ;
#38600=CARTESIAN_POINT ( 'NONE',  ( 17.14628872753620215, 12.71262973326862245, -1.500000000000002220 ) ) ;
#38601=ORIENTED_EDGE ( 'NONE', *, *, #72460, .T. ) ;
#38602=CARTESIAN_POINT ( 'NONE',  ( -14.96386864383857329, 14.77685607883014640, 11.49999999999998934 ) ) ;
#38603=CARTESIAN_POINT ( 'NONE',  ( -30.42285774359944028, -24.74858208471048471, 1.363670884829966123 ) ) ;
#38604=DIRECTION ( 'NONE',  ( -3.773278334453079030E-23, 0.9999999999976377785, 2.173523156925979128E-06 ) ) ;
#38605=CARTESIAN_POINT ( 'NONE',  ( -50.29662818668498403, -25.04370934227833700, 7.560222902623404018 ) ) ;
#38606=CARTESIAN_POINT ( 'NONE',  ( 3.092608977599853315, -21.74436839971096802, -1.500000000000002220 ) ) ;
#38607=CARTESIAN_POINT ( 'NONE',  ( -87.52287095715007581, -23.72747288104470087, -1.053458166803226126 ) ) ;
#38610=B_SPLINE_CURVE_WITH_KNOTS ( 'NONE', 3,
 ( #60010, #82327, #51386, #81832, #98536, #52384 ),
 .UNSPECIFIED., .F., .F.,
 ( 4, 2, 4 ),
 ( 0.000000000000000000, 0.001380901958385379220, 0.002761803916770758441 ),
 .UNSPECIFIED. ) ;
#38611=CARTESIAN_POINT ( 'NONE',  ( -127.5228709571500616, -23.47596703998600631, 11.44779298504227683 ) ) ;
#38612=CARTESIAN_POINT ( 'NONE',  ( 18.58881047053902691, 9.431966241625852732, 11.49999999999999645 ) ) ;
#38614=CARTESIAN_POINT ( 'NONE',  ( -86.52287095715006160, -23.47596703998600631, 11.44779298504228393 ) ) ;
#38615=CARTESIAN_POINT ( 'NONE',  ( -10.31630007230791968, -21.90547765859858842, 11.44779298504228038 ) ) ;
#38616=CARTESIAN_POINT ( 'NONE',  ( 4.979423480801214552, 20.69870207611912605, 11.49999999999998934 ) ) ;
#38617=CARTESIAN_POINT ( 'NONE',  ( -39.52287095715006870, -29.50248528299804818, 1.056150453629031594 ) ) ;
#38621=CARTESIAN_POINT ( 'NONE',  ( -20.59131556071872282, -9.131246169528550283, -1.500000000000002220 ) ) ;
#38623=ORIENTED_EDGE ( 'NONE', *, *, #55125, .F. ) ;
#38625=CARTESIAN_POINT ( 'NONE',  ( 19.39309126630920588, -2.812899550206792831, 11.49999999999999645 ) ) ;
#38629=ORIENTED_EDGE ( 'NONE', *, *, #2028, .F. ) ;
#38630=CARTESIAN_POINT ( 'NONE',  ( -88.51121366609869767, -24.15620529776628800, 10.23563542870660115 ) ) ;
#38631=CARTESIAN_POINT ( 'NONE',  ( -42.52287095715005449, -24.64965694238575011, 8.947790433994205372 ) ) ;
#38632=CARTESIAN_POINT ( 'NONE',  ( -36.62287095715005592, -23.48783264082477729, -1.443836473390072372 ) ) ;
#38633=B_SPLINE_CURVE_WITH_KNOTS ( 'NONE', 3,
 ( #14708, #33949, #56307, #39559 ),
 .UNSPECIFIED., .F., .F.,
 ( 4, 4 ),
 ( 0.000000000000000000, 9.999999999998897304E-05 ),
 .UNSPECIFIED. ) ;
#38634=CARTESIAN_POINT ( 'NONE',  ( 15.33752688427012778, 12.42672799324400934, -1.500000000000002220 ) ) ;
#38635=VECTOR ( 'NONE', #35555, 1000.000000000000114 ) ;
#38636=ORIENTED_EDGE ( 'NONE', *, *, #99387, .F. ) ;
#38640=CARTESIAN_POINT ( 'NONE',  ( -109.6228709571500275, -24.51387760970724372, 9.387446482453409402 ) ) ;
#38642=CARTESIAN_POINT ( 'NONE',  ( -78.52287095715006160, -24.64965694238408034, 8.947790433994198267 ) ) ;
#38645=EDGE_CURVE ( 'NONE', #88005, #76875, #93267, .T. ) ;
#38649=CARTESIAN_POINT ( 'NONE',  ( -15.89961544564849305, 12.09337254111102844, 11.49999999999998934 ) ) ;
#38650=EDGE_CURVE ( 'NONE', #60317, #94949, #80551, .T. ) ;
#38651=CARTESIAN_POINT ( 'NONE',  ( -45.58953762381672448, -23.47593901973091235, -1.443836447539009749 ) ) ;
#38652=CARTESIAN_POINT ( 'NONE',  ( -51.13339157368925214, -25.31518271292250688, 4.891899733068189704 ) ) ;
#38655=CARTESIAN_POINT ( 'NONE',  ( -79.58814944961092408, -24.35071581493543036, 9.817618358456028815 ) ) ;
#38656=FACE_OUTER_BOUND ( 'NONE', #76578, .T. ) ;
#38657=CARTESIAN_POINT ( 'NONE',  ( -120.6228709571500559, -24.83602698348162363, 1.605859176311272396 ) ) ;
#38658=CARTESIAN_POINT ( 'NONE',  ( -28.62287095715004881, -23.33150569529546914, 11.44779297407613150 ) ) ;
#38660=CARTESIAN_POINT ( 'NONE',  ( -83.58263009027983514, -24.65952944569305316, 1.056160979905701680 ) ) ;
#38661=B_SPLINE_SURFACE_WITH_KNOTS ( 'NONE', 3, 3, ( 
 ( #22702, #84620, #60306, #5999 ),
 ( #68406, #30331, #99339, #37455 ),
 ( #91727, #45077, #22206, #92722 ),
 ( #23210, #84120, #85118, #36949 ),
 ( #45576, #15109, #36449, #76994 ),
 ( #76493, #98839, #37947, #68897 ),
 ( #67416, #28842, #67919, #99824 ) ),
 .UNSPECIFIED., .F., .F., .F.,
 ( 4, 3, 4 ),
 ( 4, 4 ),
 ( 0.2966607060324272793, 0.4953275639659514562, 0.6939944218994755776 ),
 ( 0.04303012530936223962, 0.1472998482329709868 ),
 .UNSPECIFIED. ) ;
#38663=EDGE_CURVE ( 'NONE', #68434, #41774, #97031, .T. ) ;
#38664=CARTESIAN_POINT ( 'NONE',  ( -40.52287095715006870, -23.84081130425358808, 10.88220057483156644 ) ) ;
#38666=AXIS2_PLACEMENT_3D ( 'NONE', #95285, #80554, #26770 ) ;
#38667=CARTESIAN_POINT ( 'NONE',  ( 5.465678960246475704, -19.50585317057041124, 11.49999999999998934 ) ) ;
#38670=CARTESIAN_POINT ( 'NONE',  ( -99.62287095715005592, -24.64898659630367916, 1.056161002820829697 ) ) ;
#38671=ORIENTED_EDGE ( 'NONE', *, *, #89969, .F. ) ;
#38672=DIRECTION ( 'NONE',  ( -3.773278334453080206E-23, 0.9999999999976377785, 2.173523156925979975E-06 ) ) ;
#38673=CARTESIAN_POINT ( 'NONE',  ( 1.915021276000606454, 20.04344799065331628, -1.500000000000002220 ) ) ;
#38674=CARTESIAN_POINT ( 'NONE',  ( 11.07546443054301655, -17.96822238807187233, 11.49999999999999645 ) ) ;
#38676=CARTESIAN_POINT ( 'NONE',  ( -19.76278938440450617, -9.944092408650034187, 11.49999999999998934 ) ) ;
#38677=CARTESIAN_POINT ( 'NONE',  ( -14.38416181709762043, 14.64695106392160895, -1.500000000000002220 ) ) ;
#38678=CARTESIAN_POINT ( 'NONE',  ( -78.52287095715006160, -24.64965694238408034, 8.947790433994198267 ) ) ;
#38679=CARTESIAN_POINT ( 'NONE',  ( -126.6228709571500275, -23.94994826722566117, -0.6494450866342689199 ) ) ;
#38680=ORIENTED_EDGE ( 'NONE', *, *, #88958, .T. ) ;
#38681=DIRECTION ( 'NONE',  ( -3.773278334453079618E-23, 0.9999999999976377785, 2.173523156925979975E-06 ) ) ;
#38682=EDGE_LOOP ( 'NONE', ( #97354, #32264, #12113, #34425 ) ) ;
#38683=CARTESIAN_POINT ( 'NONE',  ( -51.62287095715005592, -24.64898659630367206, 1.056161002820821038 ) ) ;
#38684=CARTESIAN_POINT ( 'NONE',  ( -51.52287095715006870, -29.50250243563736774, 8.947779886222146928 ) ) ;
#38686=VERTEX_POINT ( 'NONE', #48625 ) ;
#38687=ORIENTED_EDGE ( 'NONE', *, *, #50775, .T. ) ;
#38689=CARTESIAN_POINT ( 'NONE',  ( -63.62287095715004881, -23.96127896941632685, -0.6493128931037893681 ) ) ;
#38690=CARTESIAN_POINT ( 'NONE',  ( -68.59250175099369073, -24.15620529776627734, 10.23563542870660825 ) ) ;
#38691=CARTESIAN_POINT ( 'NONE',  ( 20.62939718826500979, -0.8834638802319035866, -1.500000000000002220 ) ) ;
#38692=CARTESIAN_POINT ( 'NONE',  ( -14.23256820581467785, 16.29125061305494526, 11.49999999999999645 ) ) ;
#38693=EDGE_LOOP ( 'NONE', ( #33963, #36530, #14752, #89012 ) ) ;
#38694=CARTESIAN_POINT ( 'NONE',  ( -29.62287095715004881, -29.50250243563707286, 8.947779751028683393 ) ) ;
#38695=CARTESIAN_POINT ( 'NONE',  ( -60.62287095715004881, -24.99132157543084531, 2.256160258750667502 ) ) ;
#38696=CARTESIAN_POINT ( 'NONE',  ( -1.986123035288760885, 22.30159847666916662, -1.500000000000002220 ) ) ;
#38698=CARTESIAN_POINT ( 'NONE',  ( -71.52287095715009002, -23.73907113216989373, -1.053371485793249684 ) ) ;
#38699=CARTESIAN_POINT ( 'NONE',  ( -87.62287095715004170, -29.50248528299804818, 1.056150453629040253 ) ) ;
#38701=B_SPLINE_CURVE_WITH_KNOTS ( 'NONE', 3,
 ( #17168, #71473, #46130, #31899 ),
 .UNSPECIFIED., .F., .F.,
 ( 4, 4 ),
 ( 0.05982864664972729896, 0.06883507792184291596 ),
 .UNSPECIFIED. ) ;
#38703=FACE_OUTER_BOUND ( 'NONE', #80650, .T. ) ;
#38704=CARTESIAN_POINT ( 'NONE',  ( -113.5228709571500616, -29.50248528299804818, 1.056150453629043584 ) ) ;
#38705=CARTESIAN_POINT ( 'NONE',  ( 10.02768300834196502, -18.34552750054021786, 11.49999999999998934 ) ) ;
#38706=VERTEX_POINT ( 'NONE', #17151 ) ;
#38707=EDGE_CURVE ( 'NONE', #20665, #60599, #9856, .T. ) ;
#38708=CARTESIAN_POINT ( 'NONE',  ( -86.51403199199435790, -23.96119346886881374, -0.6495511937831903726 ) ) ;
#38709=ORIENTED_EDGE ( 'NONE', *, *, #15186, .T. ) ;
#38710=VECTOR ( 'NONE', #46017, 1000.000000000000114 ) ;
#38711=DIRECTION ( 'NONE',  ( 3.773278334444166432E-23, -1.000000000000000000, 0.000000000000000000 ) ) ;
#38712=CARTESIAN_POINT ( 'NONE',  ( 18.66760434907605060, -10.05535386721697222, -1.500000000000002220 ) ) ;
#38715=CARTESIAN_POINT ( 'NONE',  ( -35.52287095715008292, -25.00182538069144655, 7.747789668545105535 ) ) ;
#38716=CARTESIAN_POINT ( 'NONE',  ( -21.05831370385527990, 5.553659732266172711, -1.500000000000002220 ) ) ;
#38717=CARTESIAN_POINT ( 'NONE',  ( -113.9228709571500531, -23.47596703998600631, 11.44779298504227860 ) ) ;
#38718=CARTESIAN_POINT ( 'NONE',  ( -41.52287095715006870, -23.72747288104469732, -1.053458166803227680 ) ) ;
#38719=CARTESIAN_POINT ( 'NONE',  ( -101.6228709571500559, -23.48786465467242479, 11.44779295918254114 ) ) ;
#38720=CARTESIAN_POINT ( 'NONE',  ( 9.643594380127815668, 19.59848315111488759, -1.500000000000002220 ) ) ;
#38721=CARTESIAN_POINT ( 'NONE',  ( -30.57287095715005876, -24.05191950036741488, 10.45812762691192255 ) ) ;
#38722=ORIENTED_EDGE ( 'NONE', *, *, #79097, .T. ) ;
#38724=CARTESIAN_POINT ( 'NONE',  ( -70.22287095715006444, -23.47596703998600631, 11.44779298504227860 ) ) ;
#38726=ORIENTED_EDGE ( 'NONE', *, *, #3122, .T. ) ;
#38727=ORIENTED_EDGE ( 'NONE', *, *, #85854, .T. ) ;
#38729=CARTESIAN_POINT ( 'NONE',  ( 18.66760434907605060, -10.05535386721697222, -1.500000000000002220 ) ) ;
#38731=CARTESIAN_POINT ( 'NONE',  ( -79.05725560372792415, -25.27791764661166241, 6.604864350711941334 ) ) ;
#38734=CARTESIAN_POINT ( 'NONE',  ( 14.52268490272241408, 12.84546865777419455, 11.49999999999998934 ) ) ;
#38735=CARTESIAN_POINT ( 'NONE',  ( -40.93292953049032690, -25.30060000302003687, 6.009290021095885059 ) ) ;
#38738=CARTESIAN_POINT ( 'NONE',  ( -15.31790942089943286, 12.02624123284522106, 11.49999999999999645 ) ) ;
#38739=CARTESIAN_POINT ( 'NONE',  ( -34.62287095715004881, -23.48783264082478084, -1.443836473390074149 ) ) ;
#38741=CARTESIAN_POINT ( 'NONE',  ( -103.5228709571500758, -23.95044443724991723, 10.65354141964649237 ) ) ;
#38746=CARTESIAN_POINT ( 'NONE',  ( -76.62287095715007013, -23.47596703998600631, 11.44779298504227860 ) ) ;
#38747=CARTESIAN_POINT ( 'NONE',  ( -55.62287095715004881, -25.00158670708909625, 2.256160236439165967 ) ) ;
#38748=CARTESIAN_POINT ( 'NONE',  ( -11.98250242409135780, 15.54504917500377559, 11.49999999999998934 ) ) ;
#38751=CARTESIAN_POINT ( 'NONE',  ( -2.376235263977734657, 21.45616117177731041, 11.49999999999998934 ) ) ;
#38754=CARTESIAN_POINT ( 'NONE',  ( -40.58149357286682601, -24.73486907724916861, 1.287355809206965240 ) ) ;
#38756=CARTESIAN_POINT ( 'NONE',  ( 10.36671515591691950, -20.60271000134967068, -1.500000000000002220 ) ) ;
#38758=CARTESIAN_POINT ( 'NONE',  ( -93.52216992446560084, -23.48783264082477018, -1.443836473390090358 ) ) ;
#38759=DIRECTION ( 'NONE',  ( 1.000000000000000000, 3.773278334444167608E-23, 8.201307833595939069E-29 ) ) ;
#38760=CARTESIAN_POINT ( 'NONE',  ( -40.43800977064336877, -25.27941802265787530, 6.123089462926260218 ) ) ;
#38761=CARTESIAN_POINT ( 'NONE',  ( -39.44687923781921057, -29.50249209050310739, 4.188164501617993807 ) ) ;
#38762=EDGE_CURVE ( 'NONE', #11930, #84470, #12034, .T. ) ;
#38764=CARTESIAN_POINT ( 'NONE',  ( -111.1265005993262491, -25.10921425174257848, 3.068069789771319389 ) ) ;
#38765=B_SPLINE_CURVE_WITH_KNOTS ( 'NONE', 3,
 ( #30519, #6182, #62484, #38631 ),
 .UNSPECIFIED., .F., .F.,
 ( 4, 4 ),
 ( 0.000000000000000000, 9.999999999998900014E-05 ),
 .UNSPECIFIED. ) ;
#38767=CARTESIAN_POINT ( 'NONE',  ( -99.41873814713473223, -25.26400843806960950, 4.744921592735869886 ) ) ;
#38768=CARTESIAN_POINT ( 'NONE',  ( -4.768723929037996356, 19.30091236029735668, -1.500000000000002220 ) ) ;
#38771=CARTESIAN_POINT ( 'NONE',  ( 5.644138345009856117, 19.01542066204735448, -1.500000000000002220 ) ) ;
#38773=EDGE_CURVE ( 'NONE', #58867, #87961, #52480, .T. ) ;
#38774=B_SPLINE_CURVE_WITH_KNOTS ( 'NONE', 3,
 ( #61858, #37505, #78046, #92287, #23772, #69952 ),
 .UNSPECIFIED., .F., .F.,
 ( 4, 2, 4 ),
 ( 6.391158118956848875E-06, 0.001387004593080779424, 0.002767618028042601996 ),
 .UNSPECIFIED. ) ;
#38776=CARTESIAN_POINT ( 'NONE',  ( -73.52287095715007581, -29.50250243563736774, 8.947779886222143375 ) ) ;
#38777=CARTESIAN_POINT ( 'NONE',  ( -95.22287095715003602, -23.47593901973090169, -1.443836447538996870 ) ) ;
#38778=CARTESIAN_POINT ( 'NONE',  ( 17.22178217532253086, -11.58000449095910867, 11.49999999999999645 ) ) ;
#38779=DIRECTION ( 'NONE',  ( -3.773278334444167608E-23, 1.000000000000000000, 0.000000000000000000 ) ) ;
#38781=B_SPLINE_CURVE_WITH_KNOTS ( 'NONE', 3,
 ( #93805, #54761, #40024, #64395 ),
 .UNSPECIFIED., .F., .F.,
 ( 4, 4 ),
 ( 0.000000000000000000, 0.0001000000000000028644 ),
 .UNSPECIFIED. ) ;
#38782=CARTESIAN_POINT ( 'NONE',  ( -106.5177727992831223, -23.96119346886880663, -0.6495511937832030291 ) ) ;
#38783=CARTESIAN_POINT ( 'NONE',  ( 16.14549698687068968, 15.95341496147077720, 11.49999999999999645 ) ) ;
#38784=ORIENTED_EDGE ( 'NONE', *, *, #99973, .F. ) ;
#38785=CARTESIAN_POINT ( 'NONE',  ( -69.64548755400529956, -23.73766607897669445, -1.055555164236460008 ) ) ;
#38786=CARTESIAN_POINT ( 'NONE',  ( -106.6228709571500843, -24.50216790748207174, 0.6166512839542517277 ) ) ;
#38788=CARTESIAN_POINT ( 'NONE',  ( 19.72175082351460063, -4.362005935662174316, -1.500000000000002220 ) ) ;
#38791=DIRECTION ( 'NONE',  ( -1.000000000000000000, -3.773278334444166432E-23, -8.201307841325785021E-29 ) ) ;
#38793=ORIENTED_EDGE ( 'NONE', *, *, #15511, .F. ) ;
#38794=CARTESIAN_POINT ( 'NONE',  ( -76.62287095715007013, -29.50250243563736774, 8.947779886222141599 ) ) ;
#38795=CARTESIAN_POINT ( 'NONE',  ( 12.20170062390598709, -19.39347807479101249, 11.49999999999998934 ) ) ;
#38796=CARTESIAN_POINT ( 'NONE',  ( -51.29535283968221648, -25.27420699915789726, 3.923498428899851564 ) ) ;
#38797=CARTESIAN_POINT ( 'NONE',  ( 14.58690015069645263, 15.99052346098381250, -1.500000000000002220 ) ) ;
#38798=CARTESIAN_POINT ( 'NONE',  ( -123.5546994242114920, -24.34968618360933945, 0.1864209137778902459 ) ) ;
#38799=CARTESIAN_POINT ( 'NONE',  ( -2.368302597431856782, 20.80102113048726409, 11.49999999999999645 ) ) ;
#38800=ORIENTED_EDGE ( 'NONE', *, *, #60102, .T. ) ;
#38801=CARTESIAN_POINT ( 'NONE',  ( -124.5563175110222147, -23.73766607897670866, -1.055555164236449350 ) ) ;
#38802=CARTESIAN_POINT ( 'NONE',  ( -17.76638496452178018, -13.01238552544781335, 11.49999999999998934 ) ) ;
#38803=CARTESIAN_POINT ( 'NONE',  ( -102.2228709571500644, -23.47593901973090524, -1.443836447538996648 ) ) ;
#38805=ORIENTED_EDGE ( 'NONE', *, *, #72578, .F. ) ;
#38809=CARTESIAN_POINT ( 'NONE',  ( -72.55405769320448428, -23.96169478059712787, 10.65365249895718414 ) ) ;
#38812=VERTEX_POINT ( 'NONE', #22994 ) ;
#38814=CARTESIAN_POINT ( 'NONE',  ( -83.52287095715006160, -23.72773821059536914, 11.05748984161097503 ) ) ;
#38816=CARTESIAN_POINT ( 'NONE',  ( -15.03541999946025243, -13.88573836563254460, -1.500000000000002220 ) ) ;
#38818=EDGE_LOOP ( 'NONE', ( #14250, #6504, #1543, #38499 ) ) ;
#38819=CARTESIAN_POINT ( 'NONE',  ( -99.69921442305546577, -25.29823723214318676, 5.426898400209082318 ) ) ;
#38821=CARTESIAN_POINT ( 'NONE',  ( -44.64054379914810511, -24.15543982623906416, -0.2315651400026670914 ) ) ;
#38823=CARTESIAN_POINT ( 'NONE',  ( -17.00426676922356606, 14.40147940013276973, -1.500000000000002220 ) ) ;
#38825=CARTESIAN_POINT ( 'NONE',  ( -81.88534077628074215, -25.24685308744633616, 6.293942982122114671 ) ) ;
#38827=ORIENTED_EDGE ( 'NONE', *, *, #70524, .T. ) ;
#38828=CARTESIAN_POINT ( 'NONE',  ( -28.59999605021188884, -24.73585508254603837, 1.848451013847122626 ) ) ;
#38832=CARTESIAN_POINT ( 'NONE',  ( -1.025521031027718299, 20.81036885881322362, 11.49999999999998934 ) ) ;
#38833=ORIENTED_EDGE ( 'NONE', *, *, #97141, .F. ) ;
#38834=FACE_OUTER_BOUND ( 'NONE', #77344, .T. ) ;
#38838=CARTESIAN_POINT ( 'NONE',  ( -19.58807393344005376, -7.628504261335002923, -1.500000000000002220 ) ) ;
#38839=EDGE_CURVE ( 'NONE', #5107, #59182, #37743, .T. ) ;
#38842=CARTESIAN_POINT ( 'NONE',  ( -50.44065031394416820, -25.10935757545416891, 2.834208411262789884 ) ) ;
#38844=PLANE ( 'NONE',  #43692 ) ;
#38846=CARTESIAN_POINT ( 'NONE',  ( -100.5228709571500616, -25.00182538069145366, 7.747789668545101982 ) ) ;
#38847=CARTESIAN_POINT ( 'NONE',  ( -19.05511597014879044, -11.33806725510066826, 11.49999999999999645 ) ) ;
#38848=VERTEX_POINT ( 'NONE', #92025 ) ;
#38849=FACE_OUTER_BOUND ( 'NONE', #24371, .T. ) ;
#38851=CARTESIAN_POINT ( 'NONE',  ( -56.52287095715006870, -29.50248528299804818, 1.056150453629034924 ) ) ;
#38852=VERTEX_POINT ( 'NONE', #94025 ) ;
#38853=CARTESIAN_POINT ( 'NONE',  ( 10.43192878459595185, 20.09917060401269850, 11.49999999999998934 ) ) ;
#38854=CARTESIAN_POINT ( 'NONE',  ( -29.24562190895224489, -25.20408335486846951, 5.231737936259443167 ) ) ;
#38855=VERTEX_POINT ( 'NONE', #85410 ) ;
#38856=ORIENTED_EDGE ( 'NONE', *, *, #5204, .F. ) ;
#38859=CARTESIAN_POINT ( 'NONE',  ( -11.28321777122536140, 16.66956161807075887, 11.49999999999998934 ) ) ;
#38860=B_SPLINE_SURFACE_WITH_KNOTS ( 'NONE', 3, 1, ( 
 ( #68740, #85446 ),
 ( #22535, #69232 ),
 ( #93552, #16432 ),
 ( #92065, #76332 ),
 ( #32163, #100150 ),
 ( #713, #76822 ),
 ( #46898, #30669 ),
 ( #24549, #62131 ),
 ( #7320, #8832 ),
 ( #84949, #24046 ),
 ( #61639, #55522 ),
 ( #15932, #63136 ),
 ( #93056, #37788 ),
 ( #99658, #46396 ),
 ( #23534, #39770 ) ),
 .UNSPECIFIED., .F., .F., .F.,
 ( 4, 1, 1, 1, 1, 1, 1, 1, 1, 1, 1, 1, 4 ),
 ( 2, 2 ),
 ( 0.000000000000000000, 0.08553210767726550368, 0.1690033828897672674, 0.2519432488916409363, 0.3356820104014504591, 0.4194085858192974636, 0.5012648984817446030, 0.5837029416042844865, 0.6680003590442504802, 0.7519186598620664075, 0.8345977112584781477, 0.9165256687801534019, 1.000000000000000000 ),
 ( 0.000000000000000000, 1.000000000000000000 ),
 .UNSPECIFIED. ) ;
#38861=PLANE ( 'NONE',  #8438 ) ;
#38862=EDGE_LOOP ( 'NONE', ( #45262, #21782, #47479, #38687 ) ) ;
#38863=PLANE ( 'NONE',  #65018 ) ;
#38864=CARTESIAN_POINT ( 'NONE',  ( 8.681249458320607459, -20.60847208623538762, -1.500000000000002220 ) ) ;
#38870=CARTESIAN_POINT ( 'NONE',  ( -116.5228709571500616, -24.64965694238575011, 8.947790433994191162 ) ) ;
#38871=CARTESIAN_POINT ( 'NONE',  ( -30.61345265565988782, -24.26743686635980524, 0.04347934593174110351 ) ) ;
#38872=CARTESIAN_POINT ( 'NONE',  ( 12.07855387261060898, -15.37489856218140183, -1.500000000000002220 ) ) ;
#38874=CARTESIAN_POINT ( 'NONE',  ( 8.900169022907615357, -19.58186849131130813, -1.500000000000002220 ) ) ;
#38878=B_SPLINE_CURVE_WITH_KNOTS ( 'NONE', 3,
 ( #37857, #6904, #70813, #92631 ),
 .UNSPECIFIED., .F., .F.,
 ( 4, 4 ),
 ( 3.130749735702545926E-09, 0.004340662820791676285 ),
 .UNSPECIFIED. ) ;
#38880=CARTESIAN_POINT ( 'NONE',  ( -107.5228709571500758, -23.47596703998600631, 11.44779298504228038 ) ) ;
#38881=CARTESIAN_POINT ( 'NONE',  ( -20.58715743568940226, -9.973749938417524774, -1.500000000000002220 ) ) ;
#38885=CARTESIAN_POINT ( 'NONE',  ( 19.70663390988245922, 3.666079223618853966, 11.49999999999999645 ) ) ;
#38886=CARTESIAN_POINT ( 'NONE',  ( -109.6228709571500559, -24.66019654487199730, 8.947790411086124607 ) ) ;
#38888=AXIS2_PLACEMENT_3D ( 'NONE', #36702, #29082, #14846 ) ;
#38890=CARTESIAN_POINT ( 'NONE',  ( -103.5562042904833930, -24.64898659630528854, 1.056161002820824590 ) ) ;
#38892=ORIENTED_EDGE ( 'NONE', *, *, #25418, .T. ) ;
#38893=CARTESIAN_POINT ( 'NONE',  ( -50.62287095715007013, -24.92604778743017491, 8.074972756849360778 ) ) ;
#38894=CARTESIAN_POINT ( 'NONE',  ( -110.3139465455115129, -25.11033443737754212, 2.832404817301930056 ) ) ;
#38895=CARTESIAN_POINT ( 'NONE',  ( 6.829227106855087825, -20.66181959361685827, 11.49999999999998934 ) ) ;
#38896=CARTESIAN_POINT ( 'NONE',  ( -58.52287095715006160, -29.50248528299804818, 1.056150453629034924 ) ) ;
#38897=VECTOR ( 'NONE', #77895, 1000.000000000000114 ) ;
#38898=CARTESIAN_POINT ( 'NONE',  ( -16.92291128558595048, 9.936001969431544012, -1.500000000000002220 ) ) ;
#38899=DIRECTION ( 'NONE',  ( 0.000000000000000000, 0.9999999999976377785, 2.173523156925979975E-06 ) ) ;
#38900=B_SPLINE_CURVE_WITH_KNOTS ( 'NONE', 3,
 ( #35143, #81806, #43257, #49881, #19399, #57992 ),
 .UNSPECIFIED., .F., .F.,
 ( 4, 2, 4 ),
 ( 1.570887131794638196E-05, 0.001396322306279761073, 0.002776935741241575838 ),
 .UNSPECIFIED. ) ;
#38901=VECTOR ( 'NONE', #62830, 1000.000000000000114 ) ;
#38902=CARTESIAN_POINT ( 'NONE',  ( -109.3584176993576591, -25.27925665775238073, 4.206202527071893904 ) ) ;
#38903=EDGE_CURVE ( 'NONE', #31485, #35718, #29193, .T. ) ;
#38904=VECTOR ( 'NONE', #14580, 1000.000000000000114 ) ;
#38907=CARTESIAN_POINT ( 'NONE',  ( -3.210669876418242197, 20.33209092710186638, 11.49999999999999645 ) ) ;
#38909=EDGE_CURVE ( 'NONE', #59077, #91381, #41253, .T. ) ;
#38910=CARTESIAN_POINT ( 'NONE',  ( -120.5181857807525745, -24.52300882791530512, 0.6510814631126412566 ) ) ;
#38911=VECTOR ( 'NONE', #47360, 1000.000000000000114 ) ;
#38913=CARTESIAN_POINT ( 'NONE',  ( -70.22494714645260672, -25.12219144110276048, 7.098707458017251781 ) ) ;
#38918=CARTESIAN_POINT ( 'NONE',  ( -25.88669879221086134, -24.93063363318205461, 7.002165060778218653 ) ) ;
#38919=PLANE ( 'NONE',  #86876 ) ;
#38920=CARTESIAN_POINT ( 'NONE',  ( 5.395019145045520048, -22.42585393411717121, 11.49999999999999645 ) ) ;
#38921=CARTESIAN_POINT ( 'NONE',  ( 22.20067557195093855, 5.203973054738295190, -1.500000000000002220 ) ) ;
#38922=CARTESIAN_POINT ( 'NONE',  ( -74.63458474643041995, -24.15543982623907127, -0.2315651400026650930 ) ) ;
#38923=CARTESIAN_POINT ( 'NONE',  ( -88.52287095715004739, -23.96127896941632329, -0.6493128931038041340 ) ) ;
#38924=CARTESIAN_POINT ( 'NONE',  ( -119.5562042904834072, -24.64898659630529210, 1.056161002820831696 ) ) ;
#38925=CARTESIAN_POINT ( 'NONE',  ( 22.03792223356247604, -4.036589945906135846, 11.49999999999999645 ) ) ;
#38926=ORIENTED_EDGE ( 'NONE', *, *, #51529, .T. ) ;
#38927=CARTESIAN_POINT ( 'NONE',  ( -69.55620429048339304, -24.65952944569304606, 1.056160979905699016 ) ) ;
#38928=CARTESIAN_POINT ( 'NONE',  ( -34.62287095715005592, -24.64965695001467694, 8.947790433994189385 ) ) ;
#38929=CARTESIAN_POINT ( 'NONE',  ( 1.885617179787854036, 21.85875792104173598, -1.500000000000002220 ) ) ;
#38930=PLANE ( 'NONE',  #13768 ) ;
#38932=CARTESIAN_POINT ( 'NONE',  ( -56.58953762381673158, -23.48786465467241413, 11.44779295918254824 ) ) ;
#38933=CARTESIAN_POINT ( 'NONE',  ( -78.54308978932711227, -24.51314013834315375, 0.6176544820404143987 ) ) ;
#38934=CARTESIAN_POINT ( 'NONE',  ( -112.6228709571500417, -24.66019654487199730, 8.947790411086124607 ) ) ;
#38936=CARTESIAN_POINT ( 'NONE',  ( -15.50425215161893355, 13.37805140191733777, -1.500000000000002220 ) ) ;
#38937=VERTEX_POINT ( 'NONE', #16904 ) ;
#38939=ORIENTED_EDGE ( 'NONE', *, *, #54743, .T. ) ;
#38941=CARTESIAN_POINT ( 'NONE',  ( -22.22199965279648737, -6.226755796435518242, -1.500000000000002220 ) ) ;
#38942=CARTESIAN_POINT ( 'NONE',  ( -49.10457154551149728, -25.27419814425984512, 3.999772249604824914 ) ) ;
#38943=CARTESIAN_POINT ( 'NONE',  ( 17.44645523915803764, -10.38078700900905993, -1.500000000000002220 ) ) ;
#38944=ORIENTED_EDGE ( 'NONE', *, *, #56545, .T. ) ;
#38946=CARTESIAN_POINT ( 'NONE',  ( -92.62814048523338784, -24.34968618360935011, 0.1864209137778965741 ) ) ;
#38949=CARTESIAN_POINT ( 'NONE',  ( -70.55210020511036362, -24.15503026093916006, -0.2815557561904372674 ) ) ;
#38950=CARTESIAN_POINT ( 'NONE',  ( -20.95461191387366284, 4.708766595171775649, 11.49999999999999645 ) ) ;
#38952=CARTESIAN_POINT ( 'NONE',  ( -75.58685686046939622, -24.63355581998385802, 0.9682620441943947664 ) ) ;
#38953=CARTESIAN_POINT ( 'NONE',  ( -61.51535964669244549, -23.73791477778911840, 11.05961554403170766 ) ) ;
#38955=CARTESIAN_POINT ( 'NONE',  ( 17.22178217532253086, -11.58000449095910867, 11.49999999999998934 ) ) ;
#38956=VECTOR ( 'NONE', #30201, 1000.000000000000114 ) ;
#38959=VERTEX_POINT ( 'NONE', #86915 ) ;
#38960=EDGE_CURVE ( 'NONE', #39939, #13092, #6187, .T. ) ;
#38961=CARTESIAN_POINT ( 'NONE',  ( -111.5158189371944104, -24.35071581493544457, 9.817618358456018157 ) ) ;
#38962=CARTESIAN_POINT ( 'NONE',  ( -48.52287095715006160, -24.65952944569304606, 1.056160979905693686 ) ) ;
#38963=ORIENTED_EDGE ( 'NONE', *, *, #2752, .T. ) ;
#38964=ORIENTED_EDGE ( 'NONE', *, *, #19528, .F. ) ;
#38966=CARTESIAN_POINT ( 'NONE',  ( -42.55305635006578058, -23.96169478059712787, 10.65365249895718947 ) ) ;
#38967=B_SPLINE_CURVE_WITH_KNOTS ( 'NONE', 3,
 ( #81729, #43669, #13699, #44674 ),
 .UNSPECIFIED., .F., .F.,
 ( 4, 4 ),
 ( 1.387778780781445521E-17, 9.999999999998898659E-05 ),
 .UNSPECIFIED. ) ;
#38969=CARTESIAN_POINT ( 'NONE',  ( -15.57331531552114612, -15.56871402003811333, 11.49999999999999645 ) ) ;
#38971=CARTESIAN_POINT ( 'NONE',  ( 16.93931825803137414, 14.88162037096512158, 11.49999999999998934 ) ) ;
#38972=CARTESIAN_POINT ( 'NONE',  ( 20.40321384664088811, -4.974606123342796060, 11.49999999999998934 ) ) ;
#38976=ORIENTED_EDGE ( 'NONE', *, *, #26020, .T. ) ;
#38978=CARTESIAN_POINT ( 'NONE',  ( -32.52287095715006160, -23.48786465467240347, 11.44779295918255357 ) ) ;
#38979=EDGE_CURVE ( 'NONE', #82227, #48546, #93340, .T. ) ;
#38980=VECTOR ( 'NONE', #49263, 1000.000000000000114 ) ;
#38981=CARTESIAN_POINT ( 'NONE',  ( -90.62287095715005592, -24.82576562982392687, 8.398263435472967942 ) ) ;
#38982=ORIENTED_EDGE ( 'NONE', *, *, #16919, .F. ) ;
#38983=CARTESIAN_POINT ( 'NONE',  ( 9.152908845159860363, 19.05633030926415472, -1.500000000000002220 ) ) ;
#38985=CARTESIAN_POINT ( 'NONE',  ( -51.06671402896819956, -25.26041094286820154, 7.458179734008862916 ) ) ;
#38986=CARTESIAN_POINT ( 'NONE',  ( -49.64242587230348391, -25.29033691608420398, 4.386389768557750202 ) ) ;
#38987=DIRECTION ( 'NONE',  ( -3.773278334453080206E-23, 0.9999999999976377785, 2.173523156925979975E-06 ) ) ;
#38988=LINE ( 'NONE', #47617, #32456 ) ;
#38989=CARTESIAN_POINT ( 'NONE',  ( 19.07224962250127831, -11.27678277851665634, -1.500000000000002220 ) ) ;
#38990=CARTESIAN_POINT ( 'NONE',  ( -71.62697868567160242, -24.51314013834315730, 0.6176544820404130665 ) ) ;
#38991=EDGE_LOOP ( 'NONE', ( #100405, #93884, #18263, #27623 ) ) ;
#38992=CARTESIAN_POINT ( 'NONE',  ( -51.88058966555665563, -25.31633273641005388, 5.810524250483315001 ) ) ;
#38994=CARTESIAN_POINT ( 'NONE',  ( -126.5212072554304541, -24.15543982623907482, -0.2315651400026573492 ) ) ;
#38995=EDGE_CURVE ( 'NONE', #54673, #96355, #16394, .T. ) ;
#38996=ADVANCED_FACE ( 'NONE', ( #1693 ), #25010, .F. ) ;
#38998=CARTESIAN_POINT ( 'NONE',  ( -33.62287095715003460, -24.33927499327853639, 9.819080762295824272 ) ) ;
#38999=CARTESIAN_POINT ( 'NONE',  ( 19.29218144733592055, -2.436590042558338443, -1.500000000000002220 ) ) ;
#39001=CARTESIAN_POINT ( 'NONE',  ( 20.92345209525186078, -4.499874906010187026, 11.49999999999998934 ) ) ;
#39003=CARTESIAN_POINT ( 'NONE',  ( -60.61726691528298971, -23.48786465467241058, 11.44779295918254824 ) ) ;
#39004=CARTESIAN_POINT ( 'NONE',  ( -51.59924294399129963, -23.96119346886880663, -0.6495511937832119109 ) ) ;
#39005=CARTESIAN_POINT ( 'NONE',  ( -100.5840138597264826, -25.18440012323539179, 3.299226137916170920 ) ) ;
#39006=CARTESIAN_POINT ( 'NONE',  ( 17.32531159343115945, 14.66459048539768162, -1.500000000000002220 ) ) ;
#39009=CARTESIAN_POINT ( 'NONE',  ( 15.56394622224390645, 12.30447529683395125, 11.49999999999999645 ) ) ;
#39010=CARTESIAN_POINT ( 'NONE',  ( -51.62287095715005592, -23.47596703998600631, 11.44779298504227505 ) ) ;
#39011=CARTESIAN_POINT ( 'NONE',  ( -59.56094173781918499, -25.20074414198133539, 3.409327697718782080 ) ) ;
#39013=B_SPLINE_CURVE_WITH_KNOTS ( 'NONE', 3,
 ( #28487, #89896, #36600, #20363 ),
 .UNSPECIFIED., .F., .F.,
 ( 4, 4 ),
 ( 0.000000000000000000, 9.999999999998897304E-05 ),
 .UNSPECIFIED. ) ;
#39017=CARTESIAN_POINT ( 'NONE',  ( -115.5562042904833930, -25.00158670708909625, 2.256160236439166855 ) ) ;
#39018=CARTESIAN_POINT ( 'NONE',  ( 17.85095790706337127, 12.24325521369631176, 11.49999999999998934 ) ) ;
#39019=CARTESIAN_POINT ( 'NONE',  ( -56.48828734240129990, -24.66019654487199375, 8.947790411086122830 ) ) ;
#39020=CARTESIAN_POINT ( 'NONE',  ( -0.1161231997828221785, -19.40653004597026410, -1.500000000000002220 ) ) ;
#39021=B_SPLINE_CURVE_WITH_KNOTS ( 'NONE', 3,
 ( #38501, #46121, #13647, #14149 ),
 .UNSPECIFIED., .F., .F.,
 ( 4, 4 ),
 ( 0.000000000000000000, 1.000000000000000000 ),
 .UNSPECIFIED. ) ;
#39022=CARTESIAN_POINT ( 'NONE',  ( -55.48852725927024920, -24.63419186844611986, 9.035850630976923981 ) ) ;
#39023=CARTESIAN_POINT ( 'NONE',  ( 1.158388978951967463, 19.79969207489630634, -1.500000000000002220 ) ) ;
#39025=B_SPLINE_CURVE_WITH_KNOTS ( 'NONE', 3,
 ( #9554, #86181, #40522, #79568, #47635, #32903, #32398, #94287 ),
 .UNSPECIFIED., .F., .F.,
 ( 4, 2, 2, 4 ),
 ( -0.001224554619866341076, -0.0002241820295893607630, 0.0007761905606876195497, 0.002776935741241580175 ),
 .UNSPECIFIED. ) ;
#39026=CARTESIAN_POINT ( 'NONE',  ( -0.5597704280004801580, 20.37679164443051505, 11.49999999999999645 ) ) ;
#39027=CARTESIAN_POINT ( 'NONE',  ( -80.49410119740149128, -24.92564183028979130, 1.928384488918253536 ) ) ;
#39028=AXIS2_PLACEMENT_3D ( 'NONE', #10015, #80028, #28740 ) ;
#39030=DIRECTION ( 'NONE',  ( -3.773278334453079030E-23, 0.9999999999976377785, 2.173523156925979128E-06 ) ) ;
#39031=EDGE_CURVE ( 'NONE', #81379, #32756, #86174, .T. ) ;
#39032=ORIENTED_EDGE ( 'NONE', *, *, #82578, .T. ) ;
#39033=CARTESIAN_POINT ( 'NONE',  ( -79.53077639109011443, -25.09533482913100499, 7.254442253322116230 ) ) ;
#39034=LINE ( 'NONE', #53775, #76847 ) ;
#39035=CARTESIAN_POINT ( 'NONE',  ( -49.43920486724100982, -25.31601856400028794, 5.121422751188677402 ) ) ;
#39036=CARTESIAN_POINT ( 'NONE',  ( -66.52287095715006160, -29.50250786944525672, 11.44777988621623699 ) ) ;
#39038=CARTESIAN_POINT ( 'NONE',  ( 5.780499401231428358, -19.25771307485560158, 11.49999999999998934 ) ) ;
#39041=ORIENTED_EDGE ( 'NONE', *, *, #82193, .F. ) ;
#39042=CARTESIAN_POINT ( 'NONE',  ( -91.62287095715005592, -23.48786465467241769, 11.44779295918254114 ) ) ;
#39043=ADVANCED_FACE ( 'NONE', ( #9793 ), #71704, .F. ) ;
#39045=CARTESIAN_POINT ( 'NONE',  ( 10.67403711042701353, -20.27515232684288549, 11.49999999999999645 ) ) ;
#39046=CARTESIAN_POINT ( 'NONE',  ( 6.262736145392394427, -21.83385498489561272, -1.500000000000002220 ) ) ;
#39048=CARTESIAN_POINT ( 'NONE',  ( -45.52287095715006160, -25.00158670708908915, 2.256160236439166411 ) ) ;
#39049=LINE ( 'NONE', #77098, #47771 ) ;
#39050=CARTESIAN_POINT ( 'NONE',  ( -39.48084026492560383, -25.26931200938422961, 3.940603736575979177 ) ) ;
#39051=CARTESIAN_POINT ( 'NONE',  ( -30.57287095715006942, -23.79114969660752621, -0.9649529075300503633 ) ) ;
#39052=CARTESIAN_POINT ( 'NONE',  ( -128.6235869392866675, -24.51419770103157703, 9.386484678747171628 ) ) ;
#39053=B_SPLINE_CURVE_WITH_KNOTS ( 'NONE', 3,
 ( #27491, #96992, #59947, #34604 ),
 .UNSPECIFIED., .F., .F.,
 ( 4, 4 ),
 ( 0.000000000000000000, 9.999999999997510880E-05 ),
 .UNSPECIFIED. ) ;
#39055=ORIENTED_EDGE ( 'NONE', *, *, #32360, .T. ) ;
#39056=CARTESIAN_POINT ( 'NONE',  ( 14.85214116200856083, 13.97194181870810326, -1.500000000000002220 ) ) ;
#39057=ORIENTED_EDGE ( 'NONE', *, *, #98670, .F. ) ;
#39058=CARTESIAN_POINT ( 'NONE',  ( -19.99251892732797486, -11.32171818645973538, -1.500000000000002220 ) ) ;
#39059=FACE_OUTER_BOUND ( 'NONE', #16987, .T. ) ;
#39061=CARTESIAN_POINT ( 'NONE',  ( -101.2818275285644773, -25.17579918040796372, 6.774827964654662971 ) ) ;
#39063=ADVANCED_FACE ( 'NONE', ( #28024 ), #51361, .T. ) ;
#39064=CARTESIAN_POINT ( 'NONE',  ( -111.5228709571500758, -23.72773821059536914, 11.05748984161097326 ) ) ;
#39065=CARTESIAN_POINT ( 'NONE',  ( -21.31669061289120037, -0.5855882196083471714, 11.49999999999999645 ) ) ;
#39066=ORIENTED_EDGE ( 'NONE', *, *, #69351, .T. ) ;
#39067=VERTEX_POINT ( 'NONE', #96529 ) ;
#39068=CARTESIAN_POINT ( 'NONE',  ( 16.02632597834478645, 15.35701383120132313, -1.500000000000002220 ) ) ;
#39069=CARTESIAN_POINT ( 'NONE',  ( 11.79242832063081892, -16.95861370568002613, 11.49999999999998934 ) ) ;
#39070=ORIENTED_EDGE ( 'NONE', *, *, #86314, .T. ) ;
#39072=ADVANCED_FACE ( 'NONE', ( #87925 ), #43749, .F. ) ;
#39073=CARTESIAN_POINT ( 'NONE',  ( -109.1951039547969202, -25.27682750245845611, 4.973674001946442935 ) ) ;
#39074=CARTESIAN_POINT ( 'NONE',  ( -69.86008333542852711, -25.11539253604531297, 2.804427796191110378 ) ) ;
#39075=ORIENTED_EDGE ( 'NONE', *, *, #23318, .T. ) ;
#39076=FACE_OUTER_BOUND ( 'NONE', #78252, .T. ) ;
#39078=FACE_OUTER_BOUND ( 'NONE', #16580, .T. ) ;
#39079=FACE_OUTER_BOUND ( 'NONE', #4277, .T. ) ;
#39080=CARTESIAN_POINT ( 'NONE',  ( -17.17656601037699104, 11.78060583124977256, -1.500000000000002220 ) ) ;
#39081=CARTESIAN_POINT ( 'NONE',  ( 21.36706796925463792, 4.321743776461201669, 11.49999999999999645 ) ) ;
#39082=CARTESIAN_POINT ( 'NONE',  ( -84.62287095715005592, -24.64965695001469115, 8.947790433994182280 ) ) ;
#39084=CARTESIAN_POINT ( 'NONE',  ( -22.33494257564923302, 2.542849975942539587, 11.49999999999998934 ) ) ;
#39085=CARTESIAN_POINT ( 'NONE',  ( -118.5933811847046684, -23.48786465467241769, 11.44779295918253581 ) ) ;
#39087=CARTESIAN_POINT ( 'NONE',  ( -31.62287095715005236, -24.64965695001467694, 8.947790433994189385 ) ) ;
#39089=ORIENTED_EDGE ( 'NONE', *, *, #65844, .F. ) ;
#39093=CARTESIAN_POINT ( 'NONE',  ( 18.61059577090848549, -10.47110149595715711, -1.500000000000002220 ) ) ;
#39094=ORIENTED_EDGE ( 'NONE', *, *, #98079, .T. ) ;
#39095=CARTESIAN_POINT ( 'NONE',  ( -20.60145385712877797, -4.430719527714695793, 11.49999999999998934 ) ) ;
#39097=CARTESIAN_POINT ( 'NONE',  ( -19.25010300378637851, 5.133817055790010464, -1.500000000000002220 ) ) ;
#39098=CARTESIAN_POINT ( 'NONE',  ( -117.6228709571500417, -24.65952944569305316, 1.056160979905706121 ) ) ;
#39100=CARTESIAN_POINT ( 'NONE',  ( 0.3405503412851532130, 21.98688381012616233, -1.500000000000002220 ) ) ;
#39101=CARTESIAN_POINT ( 'NONE',  ( -107.6228709571500701, -29.50248528299804818, 1.056150453629043584 ) ) ;
#39103=DIRECTION ( 'NONE',  ( 1.000000000000000000, 3.773278334444166432E-23, 8.201307841325785021E-29 ) ) ;
#39104=EDGE_CURVE ( 'NONE', #77838, #34072, #38900, .T. ) ;
#39106=CARTESIAN_POINT ( 'NONE',  ( -10.15938669249390180, 18.18672505111813464, 11.49999999999999645 ) ) ;
#39107=EDGE_CURVE ( 'NONE', #11909, #72410, #40166, .T. ) ;
#39108=ADVANCED_FACE ( 'NONE', ( #82301 ), #61365, .T. ) ;
#39111=DIRECTION ( 'NONE',  ( 1.000000000000000000, 3.773278334444166432E-23, 8.201307841325785021E-29 ) ) ;
#39112=EDGE_CURVE ( 'NONE', #64811, #10184, #13557, .T. ) ;
#39113=CARTESIAN_POINT ( 'NONE',  ( -30.65075040189094580, -23.47621662958674804, 11.44779298504228215 ) ) ;
#39114=CARTESIAN_POINT ( 'NONE',  ( -13.45305159987462851, 16.49040971879131234, 11.49999999999998934 ) ) ;
#39115=CARTESIAN_POINT ( 'NONE',  ( -126.5228709571500616, -24.66019654487200441, 8.947790411086108620 ) ) ;
#39116=CARTESIAN_POINT ( 'NONE',  ( -27.47983700607433732, -24.97064404397603710, 2.285865536977212731 ) ) ;
#39118=DIRECTION ( 'NONE',  ( 0.000000000000000000, -2.173523156925979552E-06, 0.9999999999976378895 ) ) ;
#39119=CARTESIAN_POINT ( 'NONE',  ( 19.77564376705174709, 10.73071584254150856, -1.500000000000002220 ) ) ;
#39120=CARTESIAN_POINT ( 'NONE',  ( -109.9080821080480348, -25.30561928443788133, 5.929683345795315752 ) ) ;
#39121=VERTEX_POINT ( 'NONE', #83791 ) ;
#39122=CARTESIAN_POINT ( 'NONE',  ( -51.36387381899343296, -25.29840739023615015, 5.660634689548093235 ) ) ;
#39124=CARTESIAN_POINT ( 'NONE',  ( 11.96684523812195700, 15.63349346248531546, 11.49999999999999645 ) ) ;
#39126=CARTESIAN_POINT ( 'NONE',  ( -32.52287095715006160, -23.48786465467240347, 11.44779295918255357 ) ) ;
#39127=EDGE_CURVE ( 'NONE', #37466, #87003, #74684, .T. ) ;
#39128=ADVANCED_FACE ( 'NONE', ( #99504 ), #28899, .T. ) ;
#39129=ORIENTED_EDGE ( 'NONE', *, *, #82637, .T. ) ;
#39130=CARTESIAN_POINT ( 'NONE',  ( -99.54653831362026040, -24.65952944569304961, 1.056160979905703901 ) ) ;
#39131=CARTESIAN_POINT ( 'NONE',  ( -127.4337102941773310, -25.40067779903719014, 5.393965687396610420 ) ) ;
#39132=CARTESIAN_POINT ( 'NONE',  ( -88.86967830683752823, -25.30572777988223976, 5.920366768842380445 ) ) ;
#39134=CARTESIAN_POINT ( 'NONE',  ( 10.86211995951333620, 16.47970581058804740, 11.49999999999998934 ) ) ;
#39135=EDGE_CURVE ( 'NONE', #7254, #58462, #37636, .T. ) ;
#39136=EDGE_LOOP ( 'NONE', ( #27519, #97344, #90362, #96361 ) ) ;
#39137=CARTESIAN_POINT ( 'NONE',  ( -109.3600754929479990, -25.28541744376511247, 4.143928178231703008 ) ) ;
#39138=EDGE_CURVE ( 'NONE', #71832, #54301, #75196, .T. ) ;
#39139=AXIS2_PLACEMENT_3D ( 'NONE', #43368, #35752, #73803 ) ;
#39141=ORIENTED_EDGE ( 'NONE', *, *, #38478, .F. ) ;
#39143=DIRECTION ( 'NONE',  ( -3.773278334453079618E-23, 0.9999999999976377785, 2.173523156925979975E-06 ) ) ;
#39144=CARTESIAN_POINT ( 'NONE',  ( -70.23317170328631676, -25.30150784332992231, 5.317526772565525306 ) ) ;
#39145=CARTESIAN_POINT ( 'NONE',  ( -66.52287095715007581, -24.50216790748205398, 0.6166512839542501734 ) ) ;
#39146=DIRECTION ( 'NONE',  ( -3.773278334444167608E-23, 1.000000000000000000, 0.000000000000000000 ) ) ;
#39149=CARTESIAN_POINT ( 'NONE',  ( 2.999408428739025023, -19.78128511538675127, 11.49999999999998934 ) ) ;
#39150=EDGE_CURVE ( 'NONE', #57062, #49913, #63186, .T. ) ;
#39151=CARTESIAN_POINT ( 'NONE',  ( -99.62559895716422886, -25.10935090793326907, 3.076829667107262356 ) ) ;
#39152=CARTESIAN_POINT ( 'NONE',  ( -80.52287095715006160, -29.50247984919015209, -1.443849546365053582 ) ) ;
#39154=ADVANCED_FACE ( 'NONE', ( #84288 ), #53858, .F. ) ;
#39156=CARTESIAN_POINT ( 'NONE',  ( -79.56370193356575271, -23.48786465467241058, 11.44779295918254824 ) ) ;
#39157=CARTESIAN_POINT ( 'NONE',  ( -110.3346797185884327, -25.29012725434539277, 3.293942888057630025 ) ) ;
#39159=DIRECTION ( 'NONE',  ( -0.000000000000000000, 2.173523156925979552E-06, -0.9999999999976378895 ) ) ;
#39163=B_SPLINE_CURVE_WITH_KNOTS ( 'NONE', 3,
 ( #32509, #94404, #33016, #34516 ),
 .UNSPECIFIED., .F., .F.,
 ( 4, 4 ),
 ( 0.000000000000000000, 9.999999999996123101E-05 ),
 .UNSPECIFIED. ) ;
#39166=ORIENTED_EDGE ( 'NONE', *, *, #16248, .T. ) ;
#39167=CARTESIAN_POINT ( 'NONE',  ( 5.353267490507026771, -19.58905154090721368, -1.500000000000002220 ) ) ;
#39168=CARTESIAN_POINT ( 'NONE',  ( -114.6228709571500559, -23.47593901973091235, -1.443836447538999312 ) ) ;
#39170=CARTESIAN_POINT ( 'NONE',  ( -40.48848276756407927, -25.18740891339376731, 6.892728034667198855 ) ) ;
#39171=ORIENTED_EDGE ( 'NONE', *, *, #63135, .T. ) ;
#39172=CARTESIAN_POINT ( 'NONE',  ( -115.6228709571500559, -29.50248789122583659, 2.256150453626215580 ) ) ;
#39173=VECTOR ( 'NONE', #37032, 1000.000000000000114 ) ;
#39174=CARTESIAN_POINT ( 'NONE',  ( 10.01938154005162218, -17.43019892170380913, -1.500000000000002220 ) ) ;
#39175=CARTESIAN_POINT ( 'NONE',  ( 4.565063516603933280, 20.63981631578574039, 11.49999999999999645 ) ) ;
#39177=CARTESIAN_POINT ( 'NONE',  ( 2.710298230372018669, -21.94706154713207980, 11.49999999999998934 ) ) ;
#39178=CARTESIAN_POINT ( 'NONE',  ( 3.262959013008915665, -20.29835246810489835, -1.500000000000002220 ) ) ;
#39179=CARTESIAN_POINT ( 'NONE',  ( -60.54143455719881217, -24.52300882791528380, 0.6510814631126233820 ) ) ;
#39181=CARTESIAN_POINT ( 'NONE',  ( -116.5895376238167103, -24.64965694238408034, 8.947790433994647685 ) ) ;
#39182=ORIENTED_EDGE ( 'NONE', *, *, #34766, .T. ) ;
#39184=CARTESIAN_POINT ( 'NONE',  ( -86.52287095715006160, -23.47593901973090169, -1.443836447538996648 ) ) ;
#39185=ORIENTED_EDGE ( 'NONE', *, *, #50928, .F. ) ;
#39186=EDGE_LOOP ( 'NONE', ( #60555, #70326, #67319, #87218 ) ) ;
#39188=CARTESIAN_POINT ( 'NONE',  ( -112.6228709571500701, -23.73907113216992215, -1.053371485793222595 ) ) ;
#39189=CARTESIAN_POINT ( 'NONE',  ( -74.55620429048340725, -24.66019654487199020, 8.947790411086131712 ) ) ;
#39190=CARTESIAN_POINT ( 'NONE',  ( -68.62714824416330828, -24.51419770103157347, 9.386484678747180510 ) ) ;
#39191=CARTESIAN_POINT ( 'NONE',  ( -15.52656095410427817, -13.64048245868121434, -1.500000000000002220 ) ) ;
#39192=CARTESIAN_POINT ( 'NONE',  ( 21.36531308999010648, 3.172564587314818052, 11.49999999999999645 ) ) ;
#39193=VERTEX_POINT ( 'NONE', #59979 ) ;
#39196=CARTESIAN_POINT ( 'NONE',  ( -9.622923231576368863, -20.19340101508991125, 11.49999999999998934 ) ) ;
#39197=B_SPLINE_CURVE_WITH_KNOTS ( 'NONE', 3,
 ( #16927, #40272, #3233, #49902, #95055, #19921, #88451, #43280 ),
 .UNSPECIFIED., .F., .F.,
 ( 4, 2, 2, 4 ),
 ( 0.000000000000000000, 0.002001079623178224527, 0.003001619434767337658, 0.004002159246356450789 ),
 .UNSPECIFIED. ) ;
#39198=CARTESIAN_POINT ( 'NONE',  ( -47.53067075290624643, -24.66019654487199730, 8.947790411086117501 ) ) ;
#39199=LINE ( 'NONE', #38699, #38341 ) ;
#39200=EDGE_LOOP ( 'NONE', ( #6174, #47158, #30346, #80760 ) ) ;
#39201=CARTESIAN_POINT ( 'NONE',  ( -100.1809493305549807, -25.31121442495619789, 4.675423118741687922 ) ) ;
#39202=CARTESIAN_POINT ( 'NONE',  ( -35.56110783281771859, -23.85049219812685095, 10.88485053497527488 ) ) ;
#39203=CARTESIAN_POINT ( 'NONE',  ( -12.67655569012464944, 16.65582705476778358, -1.500000000000002220 ) ) ;
#39205=CARTESIAN_POINT ( 'NONE',  ( -45.52287095715007581, -24.14406661686763300, 10.28769366194075019 ) ) ;
#39206=ORIENTED_EDGE ( 'NONE', *, *, #71943, .F. ) ;
#39207=VECTOR ( 'NONE', #5799, 1000.000000000000114 ) ;
#39208=CARTESIAN_POINT ( 'NONE',  ( -86.62287095715004170, -29.50248528299804818, 1.056150453629040253 ) ) ;
#39209=CARTESIAN_POINT ( 'NONE',  ( -0.1268723920767304558, 21.18662008908366445, -1.500000000000002220 ) ) ;
#39210=EDGE_LOOP ( 'NONE', ( #42387, #91016, #68828, #5512 ) ) ;
#39211=PLANE ( 'NONE',  #80296 ) ;
#39213=CARTESIAN_POINT ( 'NONE',  ( -21.42251255223715134, 3.917230396363152067, 11.49999999999998934 ) ) ;
#39214=CARTESIAN_POINT ( 'NONE',  ( -121.5228709571501042, -24.51387760970724727, 9.387446482453400520 ) ) ;
#39216=CARTESIAN_POINT ( 'NONE',  ( -36.62287095715005592, -24.50216790748205042, 0.6166512839542488411 ) ) ;
#39217=CARTESIAN_POINT ( 'NONE',  ( -116.6228709571501270, -24.34917612406838927, 0.1852690917426708661 ) ) ;
#39218=CARTESIAN_POINT ( 'NONE',  ( 16.38291735060997567, -14.39268585342195905, -1.500000000000002220 ) ) ;
#39219=CARTESIAN_POINT ( 'NONE',  ( -30.57287095715005520, -24.91181100195775500, 1.926074808287914886 ) ) ;
#39220=ORIENTED_EDGE ( 'NONE', *, *, #21794, .F. ) ;
#39224=ADVANCED_FACE ( 'NONE', ( #79181 ), #18212, .T. ) ;
#39225=EDGE_CURVE ( 'NONE', #6738, #45200, #32515, .T. ) ;
#39226=ORIENTED_EDGE ( 'NONE', *, *, #44181, .T. ) ;
#39230=CARTESIAN_POINT ( 'NONE',  ( -27.83188564017057942, -24.78446414523650176, 2.282593631282324953 ) ) ;
#39232=CARTESIAN_POINT ( 'NONE',  ( 20.79131504077403747, 4.132458064796619368, -1.500000000000002220 ) ) ;
#39234=CARTESIAN_POINT ( 'NONE',  ( -71.62287095715005592, -24.66019654487199020, 8.947790411086131712 ) ) ;
#39237=CARTESIAN_POINT ( 'NONE',  ( -128.5562042904834072, -23.47593901973091235, -1.443836447538995760 ) ) ;
#39238=CARTESIAN_POINT ( 'NONE',  ( 17.72857150710123619, 7.855407458714720903, 11.49999999999998934 ) ) ;
#39239=CARTESIAN_POINT ( 'NONE',  ( -39.98262533683074338, -25.20650829394578096, 6.812666491500988464 ) ) ;
#39240=ORIENTED_EDGE ( 'NONE', *, *, #88791, .F. ) ;
#39241=CARTESIAN_POINT ( 'NONE',  ( -18.70048401425367501, 5.426029767813830063, 11.49999999999999645 ) ) ;
#39242=PLANE ( 'NONE',  #74675 ) ;
#39244=ADVANCED_FACE ( 'NONE', ( #23890 ), #9172, .F. ) ;
#39245=ORIENTED_EDGE ( 'NONE', *, *, #70090, .T. ) ;
#39246=CARTESIAN_POINT ( 'NONE',  ( -93.62287095715002749, -24.50216790748099882, 0.6166512839513739186 ) ) ;
#39247=CARTESIAN_POINT ( 'NONE',  ( -59.52287095715003318, -23.73934037231755667, 11.05740245334329330 ) ) ;
#39248=CARTESIAN_POINT ( 'NONE',  ( -106.5228709571500616, -24.50216790748204332, 0.6166512839542641622 ) ) ;
#39250=CARTESIAN_POINT ( 'NONE',  ( -93.58623170259684798, -24.51419770103157703, 9.386484678747164523 ) ) ;
#39251=CARTESIAN_POINT ( 'NONE',  ( 19.42422255247381457, -2.945173967302487039, -1.500000000000002220 ) ) ;
#39253=CARTESIAN_POINT ( 'NONE',  ( -128.5228709571500758, -29.50248528299804818, 1.056150453629047137 ) ) ;
#39255=ORIENTED_EDGE ( 'NONE', *, *, #11318, .T. ) ;
#39256=CARTESIAN_POINT ( 'NONE',  ( -8.750087785235610482, 19.73178376063210138, -1.500000000000002220 ) ) ;
#39259=CARTESIAN_POINT ( 'NONE',  ( -7.156825135384894843, 21.90021990432103038, -1.500000000000002220 ) ) ;
#39262=PLANE ( 'NONE',  #89582 ) ;
#39263=DIRECTION ( 'NONE',  ( -1.000000000000000000, -3.773278334444166432E-23, -8.201307841325785021E-29 ) ) ;
#39266=CARTESIAN_POINT ( 'NONE',  ( -129.5222683595572732, -23.48783264082477729, -1.443836473390078590 ) ) ;
#39267=AXIS2_PLACEMENT_3D ( 'NONE', #80786, #19374, #58952 ) ;
#39268=CARTESIAN_POINT ( 'NONE',  ( -99.15308351095438866, -25.31565957498872521, 4.278189846497874704 ) ) ;
#39269=CARTESIAN_POINT ( 'NONE',  ( -5.841000908416043913, -19.03464889989004050, 11.49999999999998934 ) ) ;
#39270=CARTESIAN_POINT ( 'NONE',  ( -32.62287095715004881, -23.47593901973091235, -1.443836447539013301 ) ) ;
#39271=CARTESIAN_POINT ( 'NONE',  ( 7.713363164125232707, -18.29545692620113684, -1.500000000000002220 ) ) ;
#39276=CARTESIAN_POINT ( 'NONE',  ( -20.61657899823519813, -2.091364977790679980, 11.49999999999999645 ) ) ;
#39278=B_SPLINE_CURVE_WITH_KNOTS ( 'NONE', 3,
 ( #51297, #6614, #97948, #13216 ),
 .UNSPECIFIED., .F., .F.,
 ( 4, 4 ),
 ( 0.000000000000000000, 0.0001000000000000028508 ),
 .UNSPECIFIED. ) ;
#39280=CARTESIAN_POINT ( 'NONE',  ( -106.5486723502721844, -24.65952944569304961, 1.056160979905703456 ) ) ;
#39281=CARTESIAN_POINT ( 'NONE',  ( -22.52399778787742335, 3.408274809117095572, 11.49999999999999645 ) ) ;
#39284=B_SPLINE_SURFACE_WITH_KNOTS ( 'NONE', 3, 1, ( 
 ( #29662, #99652 ),
 ( #82943, #60637 ),
 ( #91558, #14925 ),
 ( #92058, #53019 ),
 ( #22529, #43901 ),
 ( #83949, #52513 ),
 ( #91062, #30157 ),
 ( #61131, #75830 ),
 ( #36785, #76815 ),
 ( #82452, #13433 ),
 ( #44407, #53522 ),
 ( #21536, #7314 ),
 ( #69226, #67248 ),
 ( #98167, #90565 ),
 ( #75332, #7821 ),
 ( #40774, #62625 ),
 ( #86945, #30664 ),
 ( #93544, #211 ),
 ( #55012, #9823 ) ),
 .UNSPECIFIED., .F., .F., .F.,
 ( 4, 1, 1, 1, 1, 1, 1, 1, 1, 1, 1, 1, 1, 1, 1, 1, 4 ),
 ( 2, 2 ),
 ( 0.000000000000000000, 0.06443867159524530042, 0.1265469112716785804, 0.1868871534365660614, 0.2458775355894579628, 0.3040408846912645568, 0.3621912180726578612, 0.4209759327916451910, 0.4806602832796664782, 0.5406002749537588414, 0.6006890983494537206, 0.6619357897571975791, 0.7244425059139834033, 0.7890383938817431275, 0.8563137570509946617, 0.9263520282058630428, 1.000000000000000000 ),
 ( 0.000000000000000000, 1.000000000000000000 ),
 .UNSPECIFIED. ) ;
#39285=CARTESIAN_POINT ( 'NONE',  ( -69.53739244225492655, -24.65952944569304606, 1.056160979905704567 ) ) ;
#39286=B_SPLINE_CURVE_WITH_KNOTS ( 'NONE', 3,
 ( #11895, #4293, #89029, #42864 ),
 .UNSPECIFIED., .F., .F.,
 ( 4, 4 ),
 ( 3.876650091915111752E-09, 0.002303383447661763554 ),
 .UNSPECIFIED. ) ;
#39288=ORIENTED_EDGE ( 'NONE', *, *, #27731, .T. ) ;
#39289=CARTESIAN_POINT ( 'NONE',  ( 8.473373031455752269, -18.34320851062214430, 11.49999999999998934 ) ) ;
#39290=FACE_OUTER_BOUND ( 'NONE', #67810, .T. ) ;
#39291=CARTESIAN_POINT ( 'NONE',  ( -40.73433408427551683, -25.30552906146762027, 5.044818317511085226 ) ) ;
#39293=ORIENTED_EDGE ( 'NONE', *, *, #20480, .T. ) ;
#39294=CARTESIAN_POINT ( 'NONE',  ( -127.5228709571500900, -24.34917612406837861, 0.1852690917426607076 ) ) ;
#39295=CARTESIAN_POINT ( 'NONE',  ( 15.42672287639063100, 16.92133821996916865, 11.49999999999998934 ) ) ;
#39296=CARTESIAN_POINT ( 'NONE',  ( -41.80014015042835496, -25.25166947788726191, 3.754039313533760858 ) ) ;
#39297=CARTESIAN_POINT ( 'NONE',  ( -15.70146493180990888, -14.86199287721409590, -1.500000000000002220 ) ) ;
#39299=VECTOR ( 'NONE', #28782, 1000.000000000000114 ) ;
#39300=CARTESIAN_POINT ( 'NONE',  ( 2.299058169534009100, 20.76012671103276475, 11.49999999999999645 ) ) ;
#39301=ORIENTED_EDGE ( 'NONE', *, *, #15326, .T. ) ;
#39302=CARTESIAN_POINT ( 'NONE',  ( -61.25483235428281148, -25.21329443217976873, 6.713654904961149583 ) ) ;
#39303=CARTESIAN_POINT ( 'NONE',  ( -68.93918693012690824, -25.24754535617828921, 6.184868461386431093 ) ) ;
#39304=CARTESIAN_POINT ( 'NONE',  ( -20.87105610827876134, -7.033761084331515256, -1.500000000000002220 ) ) ;
#39307=ORIENTED_EDGE ( 'NONE', *, *, #77120, .F. ) ;
#39310=ORIENTED_EDGE ( 'NONE', *, *, #95831, .T. ) ;
#39314=CARTESIAN_POINT ( 'NONE',  ( -106.6228709571500275, -24.51283580621364067, 0.6167428607019890263 ) ) ;
#39317=CARTESIAN_POINT ( 'NONE',  ( -20.46784169311667867, 0.4426517378232717737, -1.500000000000002220 ) ) ;
#39318=ORIENTED_EDGE ( 'NONE', *, *, #73619, .F. ) ;
#39319=CARTESIAN_POINT ( 'NONE',  ( -71.62287095715005592, -24.35013146730204170, 9.818937971375111928 ) ) ;
#39320=CARTESIAN_POINT ( 'NONE',  ( -44.60008626239309848, -23.96119346886879597, -0.6495511937832129101 ) ) ;
#39321=CARTESIAN_POINT ( 'NONE',  ( -77.52287095715006160, -24.64898659630367916, 1.056161002820826145 ) ) ;
#39322=CARTESIAN_POINT ( 'NONE',  ( -8.840690135214121170, 20.45858245768130956, -1.500000000000002220 ) ) ;
#39324=CARTESIAN_POINT ( 'NONE',  ( -55.52287095715006160, -24.83620972994591014, 8.398175272781369216 ) ) ;
#39325=CARTESIAN_POINT ( 'NONE',  ( -27.70544111104076990, -24.64017222881049207, 8.251826729410561612 ) ) ;
#39328=CARTESIAN_POINT ( 'NONE',  ( -29.77636857527935277, -24.63645529384542954, 5.788904288867858128 ) ) ;
#39330=CARTESIAN_POINT ( 'NONE',  ( -20.33245250387252767, 4.503473919074798104, -1.500000000000002220 ) ) ;
#39332=DIRECTION ( 'NONE',  ( -1.000000000000000000, -3.773278334444167608E-23, -8.201307833595939069E-29 ) ) ;
#39333=ORIENTED_EDGE ( 'NONE', *, *, #84712, .F. ) ;
#39334=B_SPLINE_CURVE_WITH_KNOTS ( 'NONE', 3,
 ( #7127, #38077, #69032, #99960 ),
 .UNSPECIFIED., .F., .F.,
 ( 4, 4 ),
 ( 0.000000000000000000, 9.999999999998897304E-05 ),
 .UNSPECIFIED. ) ;
#39336=VECTOR ( 'NONE', #10571, 1000.000000000000114 ) ;
#39337=CARTESIAN_POINT ( 'NONE',  ( -58.52287095715006870, -23.95044443724993144, 10.65354141964648882 ) ) ;
#39338=CARTESIAN_POINT ( 'NONE',  ( 18.89479412359299815, 9.153864009170110450, -1.500000000000002220 ) ) ;
#39339=ORIENTED_EDGE ( 'NONE', *, *, #8881, .T. ) ;
#39341=CARTESIAN_POINT ( 'NONE',  ( -55.62287095715004881, -24.82576562982391621, 8.398263435472967942 ) ) ;
#39344=VECTOR ( 'NONE', #72080, 1000.000000000000114 ) ;
#39345=DIRECTION ( 'NONE',  ( -3.773278334453079618E-23, 0.9999999999976377785, 2.173523156925979975E-06 ) ) ;
#39347=CARTESIAN_POINT ( 'NONE',  ( -59.50360827014927168, -24.15543982623906416, -0.2315651400026668416 ) ) ;
#39349=CARTESIAN_POINT ( 'NONE',  ( 16.02632597834478645, 15.35701383120132313, 11.49999999999999645 ) ) ;
#39353=ORIENTED_EDGE ( 'NONE', *, *, #58876, .F. ) ;
#39355=CARTESIAN_POINT ( 'NONE',  ( -22.46375958613465684, 3.124547546656453179, -1.500000000000002220 ) ) ;
#39356=ADVANCED_FACE ( 'NONE', ( #50747 ), #17794, .T. ) ;
#39357=CARTESIAN_POINT ( 'NONE',  ( -28.37391457004085638, -24.89382844618185331, 7.412098205223180081 ) ) ;
#39359=ADVANCED_FACE ( 'NONE', ( #65495 ), #73582, .T. ) ;
#39360=ORIENTED_EDGE ( 'NONE', *, *, #74673, .T. ) ;
#39362=FACE_OUTER_BOUND ( 'NONE', #6065, .T. ) ;
#39364=B_SPLINE_CURVE_WITH_KNOTS ( 'NONE', 3,
 ( #78107, #79623, #55810, #49201 ),
 .UNSPECIFIED., .F., .F.,
 ( 4, 4 ),
 ( 2.677034095660378764E-09, 0.001652431040122505791 ),
 .UNSPECIFIED. ) ;
#39365=CARTESIAN_POINT ( 'NONE',  ( 7.141438900065890216, -18.84860497471923679, 11.49999999999998934 ) ) ;
#39367=ORIENTED_EDGE ( 'NONE', *, *, #19528, .T. ) ;
#39368=CARTESIAN_POINT ( 'NONE',  ( -80.96226385320385077, -25.14083923594767001, 2.947789366383926968 ) ) ;
#39369=CARTESIAN_POINT ( 'NONE',  ( -14.53400517605410158, 16.95891092046126403, -1.500000000000002220 ) ) ;
#39370=ORIENTED_EDGE ( 'NONE', *, *, #67200, .T. ) ;
#39372=CARTESIAN_POINT ( 'NONE',  ( -29.62287095715004881, -29.50250786944496539, 11.44777975102276812 ) ) ;
#39375=LINE ( 'NONE', #61730, #2049 ) ;
#39376=CARTESIAN_POINT ( 'NONE',  ( -57.52287095715005449, -24.64965694238407323, 8.947790433994201820 ) ) ;
#39377=CARTESIAN_POINT ( 'NONE',  ( -63.93900422158343844, -24.04615231314291535, -0.4716817114508916609 ) ) ;
#39378=CARTESIAN_POINT ( 'NONE',  ( -0.4769873229303308038, -19.55164744950295841, 11.49999999999998934 ) ) ;
#39381=CARTESIAN_POINT ( 'NONE',  ( 15.57385778016992894, -14.83193121981731544, 11.49999999999998934 ) ) ;
#39383=DIRECTION ( 'NONE',  ( -3.773278334453079618E-23, 0.9999999999976377785, 2.173523156925979975E-06 ) ) ;
#39386=CARTESIAN_POINT ( 'NONE',  ( 19.70479270790718829, 11.56945388388114360, -1.500000000000002220 ) ) ;
#39387=B_SPLINE_CURVE_WITH_KNOTS ( 'NONE', 3,
 ( #35604, #66575, #90873, #97488 ),
 .UNSPECIFIED., .F., .F.,
 ( 4, 4 ),
 ( 0.9104360445717412098, 0.9194424758438565215 ),
 .UNSPECIFIED. ) ;
#39389=DIRECTION ( 'NONE',  ( 0.000000000000000000, -2.173523156925980399E-06, 0.9999999999976378895 ) ) ;
#39390=CARTESIAN_POINT ( 'NONE',  ( -53.60569991856895911, -23.73766607897669090, -1.055555164236459564 ) ) ;
#39391=CARTESIAN_POINT ( 'NONE',  ( -18.81269933604069067, 6.858547123926768130, 11.49999999999999645 ) ) ;
#39392=CARTESIAN_POINT ( 'NONE',  ( -100.2228709571500787, -23.47593901973090169, -1.443836447538996870 ) ) ;
#39395=DIRECTION ( 'NONE',  ( -3.773278334453079618E-23, 0.9999999999976377785, 2.173523156925979975E-06 ) ) ;
#39398=CARTESIAN_POINT ( 'NONE',  ( -13.65724274058436194, -16.95215541261048742, 11.49999999999998934 ) ) ;
#39400=CARTESIAN_POINT ( 'NONE',  ( -16.08770303010339831, 11.32657509950784736, -1.500000000000002220 ) ) ;
#39402=B_SPLINE_CURVE_WITH_KNOTS ( 'NONE', 3,
 ( #8939, #31779, #326, #62750, #94673, #32276 ),
 .UNSPECIFIED., .F., .F.,
 ( 4, 2, 4 ),
 ( 0.000000000000000000, 0.001380764517854765399, 0.002761529035709530799 ),
 .UNSPECIFIED. ) ;
#39404=CARTESIAN_POINT ( 'NONE',  ( -41.46432051929361506, -25.27404221065474843, 4.124998039036684716 ) ) ;
#39408=CARTESIAN_POINT ( 'NONE',  ( -73.62287095715007013, -24.66019654487199020, 8.947790411086131712 ) ) ;
#39409=CARTESIAN_POINT ( 'NONE',  ( 20.52540449432101610, 0.9483640940595650104, 11.49999999999999645 ) ) ;
#39412=LINE ( 'NONE', #24178, #54589 ) ;
#39414=CARTESIAN_POINT ( 'NONE',  ( 18.79633983808273712, -12.56333175589740847, 11.49999999999999645 ) ) ;
#39415=EDGE_LOOP ( 'NONE', ( #65100, #11747, #36091, #2186 ) ) ;
#39416=EDGE_CURVE ( 'NONE', #73037, #95392, #21993, .T. ) ;
#39417=CARTESIAN_POINT ( 'NONE',  ( -99.53249707683190195, -25.31296311462813975, 4.095394517951907787 ) ) ;
#39418=CARTESIAN_POINT ( 'NONE',  ( -37.52287095715006870, -24.64898659630367206, 1.056161002820819261 ) ) ;
#39419=CARTESIAN_POINT ( 'NONE',  ( -125.5890726425938055, -24.83644354573579349, 8.397322867130096569 ) ) ;
#39422=CARTESIAN_POINT ( 'NONE',  ( -33.62287095715007013, -24.33832256527048088, 0.1851278514138572917 ) ) ;
#39423=CARTESIAN_POINT ( 'NONE',  ( -75.55620429048340725, -23.47593901973091235, -1.443836447539004642 ) ) ;
#39425=CARTESIAN_POINT ( 'NONE',  ( 1.912052097559287844, -22.98750448113701239, 11.49999999999999645 ) ) ;
#39426=CARTESIAN_POINT ( 'NONE',  ( 21.14626179850551324, 8.528272852130310611, -1.500000000000002220 ) ) ;
#39428=B_SPLINE_SURFACE_WITH_KNOTS ( 'NONE', 3, 1, ( 
 ( #29739, #84019 ),
 ( #6899, #60706 ),
 ( #91627, #14506 ),
 ( #76396, #88032 ),
 ( #95639, #18010 ),
 ( #17004, #48973 ),
 ( #78395, #79904 ),
 ( #26124, #10904 ),
 ( #2301, #96144 ),
 ( #55590, #41867 ),
 ( #34245, #9894 ),
 ( #24610, #8898 ),
 ( #65220, #32731 ),
 ( #71307, #40353 ),
 ( #39844, #25111 ),
 ( #26631, #88528 ),
 ( #1792, #72811 ),
 ( #17510, #57095 ),
 ( #94631, #57591 ) ),
 .UNSPECIFIED., .F., .F., .F.,
 ( 4, 1, 1, 1, 1, 1, 1, 1, 1, 1, 1, 1, 1, 1, 1, 1, 4 ),
 ( 2, 2 ),
 ( 0.000000000000000000, 0.06554117033740432252, 0.1289631677825942568, 0.1903771361885626123, 0.2500923616690557960, 0.3085484324592007166, 0.3663979630552985367, 0.4245421892666791930, 0.4831699964229071442, 0.5422433998311213532, 0.6017393520173313082, 0.6625060022496070955, 0.7248555134488467999, 0.7891278292811820805, 0.8563463998785099118, 0.9262952349869061353, 1.000000000000000000 ),
 ( 0.000000000000000000, 1.000000000000000000 ),
 .UNSPECIFIED. ) ;
#39429=CARTESIAN_POINT ( 'NONE',  ( -72.62287095715005592, -24.66019654487199020, 8.947790411086131712 ) ) ;
#39430=CARTESIAN_POINT ( 'NONE',  ( -35.52287095715006870, -23.47593901973090169, -1.443836447538997092 ) ) ;
#39431=CARTESIAN_POINT ( 'NONE',  ( 19.55810785529653373, 10.91776788121007868, 11.49999999999999645 ) ) ;
#39432=VERTEX_POINT ( 'NONE', #95415 ) ;
#39433=CARTESIAN_POINT ( 'NONE',  ( -125.6228709571500275, -23.48783264082479505, -1.443836473390057273 ) ) ;
#39434=DIRECTION ( 'NONE',  ( 0.000000000000000000, -0.9999999999976377785, -2.173523156925979128E-06 ) ) ;
#39435=CARTESIAN_POINT ( 'NONE',  ( 20.73430856240977249, 7.200853762728330665, 11.49999999999998934 ) ) ;
#39438=CARTESIAN_POINT ( 'NONE',  ( -34.52670523829452520, -24.66019654487199730, 8.947790411086117501 ) ) ;
#39440=ORIENTED_EDGE ( 'NONE', *, *, #33550, .T. ) ;
#39441=CARTESIAN_POINT ( 'NONE',  ( -98.62287095715005592, -29.50247984919015209, -1.443849546365050029 ) ) ;
#39443=ORIENTED_EDGE ( 'NONE', *, *, #78866, .T. ) ;
#39444=CARTESIAN_POINT ( 'NONE',  ( 16.11427877760282001, 12.65940972936023812, -1.500000000000002220 ) ) ;
#39446=ORIENTED_EDGE ( 'NONE', *, *, #50517, .T. ) ;
#39450=CARTESIAN_POINT ( 'NONE',  ( 18.43541038833219758, -13.85303862407246811, -1.500000000000002220 ) ) ;
#39451=CARTESIAN_POINT ( 'NONE',  ( -41.47855695116675889, -25.26871255744267231, 3.880430150159563496 ) ) ;
#39452=CARTESIAN_POINT ( 'NONE',  ( -2.356373108420451334, 20.14613781377289214, -1.500000000000002220 ) ) ;
#39455=CARTESIAN_POINT ( 'NONE',  ( -128.6228709571500417, -29.50250243563736774, 8.947779886222132717 ) ) ;
#39456=CARTESIAN_POINT ( 'NONE',  ( -92.62572919848177833, -24.51314013834316796, 0.6176544820404266112 ) ) ;
#39459=CARTESIAN_POINT ( 'NONE',  ( -16.43003769262999469, -13.82051474754189258, 11.49999999999999645 ) ) ;
#39460=ORIENTED_EDGE ( 'NONE', *, *, #58743, .T. ) ;
#39461=CARTESIAN_POINT ( 'NONE',  ( -75.62366544631902343, -25.00158670708910691, 2.256160236439223699 ) ) ;
#39462=CARTESIAN_POINT ( 'NONE',  ( -61.53885010291545399, -24.51419770103157347, 9.386484678747178734 ) ) ;
#39465=CARTESIAN_POINT ( 'NONE',  ( 1.902724757927627408, 20.64897553884969028, 11.49999999999998934 ) ) ;
#39466=ORIENTED_EDGE ( 'NONE', *, *, #83004, .T. ) ;
#39469=CARTESIAN_POINT ( 'NONE',  ( -111.5524794374848625, -24.35071581493544457, 9.817618358456018157 ) ) ;
#39471=ORIENTED_EDGE ( 'NONE', *, *, #1901, .F. ) ;
#39473=CARTESIAN_POINT ( 'NONE',  ( -40.52287095715005449, -25.00158670708908915, 2.256160236439166411 ) ) ;
#39474=CARTESIAN_POINT ( 'NONE',  ( -42.52914555497864058, -24.66019654487198665, 8.947790411086131712 ) ) ;
#39476=CARTESIAN_POINT ( 'NONE',  ( 19.92286461850947887, -9.344431347164146473, 11.49999999999999645 ) ) ;
#39478=LINE ( 'NONE', #24740, #17195 ) ;
#39479=CARTESIAN_POINT ( 'NONE',  ( -10.21242994381667657, -20.12718729479640700, 11.49999999999998934 ) ) ;
#39480=CARTESIAN_POINT ( 'NONE',  ( -10.24336464640716216, -18.35016636821181280, -1.500000000000002220 ) ) ;
#39483=CARTESIAN_POINT ( 'NONE',  ( -99.29687923781919778, -25.26138073939643292, 6.149712181314777482 ) ) ;
#39484=ORIENTED_EDGE ( 'NONE', *, *, #19991, .T. ) ;
#39486=VERTEX_POINT ( 'NONE', #3083 ) ;
#39487=ADVANCED_FACE ( 'NONE', ( #50250 ), #80192, .F. ) ;
#39491=EDGE_LOOP ( 'NONE', ( #62425, #55688, #67121, #86094 ) ) ;
#39492=CARTESIAN_POINT ( 'NONE',  ( 20.45381123341165619, -5.387677532796200097, -1.500000000000002220 ) ) ;
#39494=CARTESIAN_POINT ( 'NONE',  ( -50.40895856474225667, -25.26041117107507006, 7.563173721887078038 ) ) ;
#39495=FACE_OUTER_BOUND ( 'NONE', #83152, .T. ) ;
#39497=CARTESIAN_POINT ( 'NONE',  ( -122.5228709571500616, -29.50250243563736774, 8.947779886222134493 ) ) ;
#39498=CARTESIAN_POINT ( 'NONE',  ( 10.50125231818214289, 19.49540335892314502, -1.500000000000002220 ) ) ;
#39500=CARTESIAN_POINT ( 'NONE',  ( -81.50937295599044319, -24.15620529776628089, 10.23563542870661180 ) ) ;
#39501=EDGE_CURVE ( 'NONE', #68398, #34688, #42519, .T. ) ;
#39503=CARTESIAN_POINT ( 'NONE',  ( -82.62287095715004170, -23.47596703998600631, 11.44779298504227860 ) ) ;
#39504=CARTESIAN_POINT ( 'NONE',  ( -37.55289829746592289, -23.96119346886880663, -0.6495511937831990323 ) ) ;
#39506=CARTESIAN_POINT ( 'NONE',  ( -75.92287095715006728, -23.47593901973090169, -1.443836447538997536 ) ) ;
#39508=CARTESIAN_POINT ( 'NONE',  ( 4.201609111248720829, -18.99613120386805676, -1.500000000000002220 ) ) ;
#39509=CARTESIAN_POINT ( 'NONE',  ( 6.029407872858970840, -20.54391778677962677, -1.500000000000002220 ) ) ;
#39511=CARTESIAN_POINT ( 'NONE',  ( -60.58331481027634879, -24.73531770709804078, 8.716586749031112191 ) ) ;
#39513=CARTESIAN_POINT ( 'NONE',  ( -44.52287095715005449, -23.95044443724991723, 10.65354141964648882 ) ) ;
#39514=CARTESIAN_POINT ( 'NONE',  ( 4.020035926878589905, 22.33396232419688587, -1.500000000000002220 ) ) ;
#39515=CARTESIAN_POINT ( 'NONE',  ( -98.63501208860351710, -23.73766607897669445, -1.055555164236453569 ) ) ;
#39517=CARTESIAN_POINT ( 'NONE',  ( 15.03354914759215966, -12.96403794047452607, 11.49999999999999645 ) ) ;
#39519=PLANE ( 'NONE',  #97612 ) ;
#39520=CARTESIAN_POINT ( 'NONE',  ( -40.94687923781921768, -29.50249942614373921, 7.563164501610022405 ) ) ;
#39521=ORIENTED_EDGE ( 'NONE', *, *, #32273, .F. ) ;
#39525=CARTESIAN_POINT ( 'NONE',  ( -51.19185979282234200, -25.27412279900076797, 3.072503657614854777 ) ) ;
#39526=CARTESIAN_POINT ( 'NONE',  ( -0.4625342273119020797, 21.68341340789531912, -1.500000000000002220 ) ) ;
#39527=CARTESIAN_POINT ( 'NONE',  ( -56.53760808179874431, -24.51419770103157347, 9.386484678747180510 ) ) ;
#39528=CARTESIAN_POINT ( 'NONE',  ( 18.45204572605500104, 6.281640480902235701, -1.500000000000002220 ) ) ;
#39529=CARTESIAN_POINT ( 'NONE',  ( -123.6228709571500701, -23.96177878511308634, 10.65340807706329684 ) ) ;
#39530=EDGE_CURVE ( 'NONE', #81255, #89515, #11667, .T. ) ;
#39531=VERTEX_POINT ( 'NONE', #18780 ) ;
#39533=CARTESIAN_POINT ( 'NONE',  ( -18.95781532540867076, -7.450117396690965066, 11.49999999999999645 ) ) ;
#39534=CARTESIAN_POINT ( 'NONE',  ( -80.62364778154437772, -25.00158670708910691, 2.256160236439221034 ) ) ;
#39535=EDGE_CURVE ( 'NONE', #8654, #69272, #12294, .T. ) ;
#39538=CARTESIAN_POINT ( 'NONE',  ( -79.99253962700090881, -25.04791361497069957, 7.492507233463702399 ) ) ;
#39539=CARTESIAN_POINT ( 'NONE',  ( -29.62287095715004526, -24.27255113093383088, 0.1850815668343412101 ) ) ;
#39540=CARTESIAN_POINT ( 'NONE',  ( -48.99007696559036162, -25.31601964366231172, 5.618156375692663573 ) ) ;
#39541=CARTESIAN_POINT ( 'NONE',  ( -40.47471336972785139, -24.83644354573577928, 8.397322867130096569 ) ) ;
#39542=CARTESIAN_POINT ( 'NONE',  ( -89.40841769935767047, -25.05712065398430966, 7.447789548358837663 ) ) ;
#39543=CARTESIAN_POINT ( 'NONE',  ( 6.297820759360134524, 19.07352124001985771, -1.500000000000002220 ) ) ;
#39544=B_SPLINE_CURVE_WITH_KNOTS ( 'NONE', 3,
 ( #72756, #26065, #95577, #59027 ),
 .UNSPECIFIED., .F., .F.,
 ( 4, 4 ),
 ( 0.000000000000000000, 0.0001000000000000028644 ),
 .UNSPECIFIED. ) ;
#39546=ORIENTED_EDGE ( 'NONE', *, *, #83621, .T. ) ;
#39547=CARTESIAN_POINT ( 'NONE',  ( -36.52287095715007581, -23.72747288104469732, -1.053458166803228124 ) ) ;
#39548=CARTESIAN_POINT ( 'NONE',  ( -2.941484630304247450, -22.72858670154147376, 11.49999999999999645 ) ) ;
#39549=CARTESIAN_POINT ( 'NONE',  ( -16.51154719052397724, 15.62863258182435189, 11.49999999999998934 ) ) ;
#39550=ORIENTED_EDGE ( 'NONE', *, *, #50040, .T. ) ;
#39551=CARTESIAN_POINT ( 'NONE',  ( -109.6228709571500417, -23.48783264082478794, -1.443836473390060382 ) ) ;
#39552=CARTESIAN_POINT ( 'NONE',  ( -97.58953762381672448, -23.47593901973091235, -1.443836447539001089 ) ) ;
#39553=CARTESIAN_POINT ( 'NONE',  ( -39.44687923781921057, -25.28830591450888221, 4.188173661249233959 ) ) ;
#39557=B_SPLINE_CURVE_WITH_KNOTS ( 'NONE', 3,
 ( #3315, #96145, #19505, #34246 ),
 .UNSPECIFIED., .F., .F.,
 ( 4, 4 ),
 ( 0.5301645019713113749, 0.5391709332434267976 ),
 .UNSPECIFIED. ) ;
#39558=CARTESIAN_POINT ( 'NONE',  ( -128.5214463091758716, -24.51419770103157703, 9.386484678747171628 ) ) ;
#39559=CARTESIAN_POINT ( 'NONE',  ( -34.62287095715005592, -24.65952944569303895, 1.056160979905691688 ) ) ;
#39561=CARTESIAN_POINT ( 'NONE',  ( -5.191926799570463658, 19.71030214607805675, -1.500000000000002220 ) ) ;
#39564=CARTESIAN_POINT ( 'NONE',  ( -14.90462150274475306, 17.49973755783957685, -1.500000000000002220 ) ) ;
#39566=CARTESIAN_POINT ( 'NONE',  ( -88.52287095715007581, -24.50216790748205398, 0.6166512839542540592 ) ) ;
#39568=VERTEX_POINT ( 'NONE', #90799 ) ;
#39569=CARTESIAN_POINT ( 'NONE',  ( -122.5228709571500616, -24.65952944569305316, 1.056160979905705899 ) ) ;
#39571=CARTESIAN_POINT ( 'NONE',  ( -6.620899627221215944, -20.26055204357936290, 11.49999999999999645 ) ) ;
#39573=ORIENTED_EDGE ( 'NONE', *, *, #85319, .F. ) ;
#39574=CARTESIAN_POINT ( 'NONE',  ( -14.87450875942801254, -16.50811611944624602, -1.500000000000002220 ) ) ;
#39575=CARTESIAN_POINT ( 'NONE',  ( 20.50092990308456464, -2.467789585553555654, -1.500000000000002220 ) ) ;
#39578=CARTESIAN_POINT ( 'NONE',  ( -112.6228709571500559, -24.64965695001469115, 8.947790433994176951 ) ) ;
#39579=CARTESIAN_POINT ( 'NONE',  ( -95.58652046637003252, -24.73531770709095312, 8.716586749053508498 ) ) ;
#39581=CARTESIAN_POINT ( 'NONE',  ( -111.9228709571500673, -23.47593901973090524, -1.443836447538996648 ) ) ;
#39582=ORIENTED_EDGE ( 'NONE', *, *, #18835, .F. ) ;
#39583=CARTESIAN_POINT ( 'NONE',  ( -93.62287095715005592, -23.47593901973091235, -1.443836447539002865 ) ) ;
#39584=CARTESIAN_POINT ( 'NONE',  ( -115.9228709571500673, -23.47596703998600631, 11.44779298504227860 ) ) ;
#39585=CARTESIAN_POINT ( 'NONE',  ( 12.70736309587848645, -16.60074808024427284, -1.500000000000002220 ) ) ;
#39586=EDGE_CURVE ( 'NONE', #74711, #97718, #52245, .T. ) ;
#39587=CARTESIAN_POINT ( 'NONE',  ( 19.92038474643397805, 8.973206291307779026, 11.49999999999999645 ) ) ;
#39588=CARTESIAN_POINT ( 'NONE',  ( -27.07602811445854130, -24.89279971831744831, 7.457967357350439919 ) ) ;
#39589=CARTESIAN_POINT ( 'NONE',  ( -99.05895993289298929, -25.17595066986875807, 6.775462437080328471 ) ) ;
#39590=CARTESIAN_POINT ( 'NONE',  ( 22.44084908143146251, -0.7541981612834567361, -1.500000000000002220 ) ) ;
#39591=CARTESIAN_POINT ( 'NONE',  ( -118.5191024237056325, -24.15620529776628800, 10.23563542870659759 ) ) ;
#39594=ORIENTED_EDGE ( 'NONE', *, *, #78333, .F. ) ;
#39598=CARTESIAN_POINT ( 'NONE',  ( -21.18999663186871274, 2.814949255606389311, -1.500000000000002220 ) ) ;
#39599=CARTESIAN_POINT ( 'NONE',  ( -22.26391555059773353, 2.265117081278330780, 11.49999999999999645 ) ) ;
#39600=ORIENTED_EDGE ( 'NONE', *, *, #57924, .F. ) ;
#39601=CARTESIAN_POINT ( 'NONE',  ( 3.661087877195506213, -20.73962600213626217, 11.49999999999998934 ) ) ;
#39602=DIRECTION ( 'NONE',  ( -3.773278334453079030E-23, 0.9999999999976377785, 2.173523156925979128E-06 ) ) ;
#39603=CARTESIAN_POINT ( 'NONE',  ( 12.75013301566243129, -15.34773647900153115, -1.500000000000002220 ) ) ;
#39605=CARTESIAN_POINT ( 'NONE',  ( -49.28939602672390663, -25.12437686555682248, 7.151409255195910752 ) ) ;
#39606=CARTESIAN_POINT ( 'NONE',  ( -10.95654650054425794, 19.06054500580150446, -1.500000000000002220 ) ) ;
#39608=ORIENTED_EDGE ( 'NONE', *, *, #27446, .F. ) ;
#39609=CARTESIAN_POINT ( 'NONE',  ( -39.52287095715006870, -23.47593901973090524, -1.443836447538997092 ) ) ;
#39611=CARTESIAN_POINT ( 'NONE',  ( -70.55620429048340725, -23.47593901973091235, -1.443836447539006196 ) ) ;
#39612=CARTESIAN_POINT ( 'NONE',  ( -20.82185584224439978, -0.2524610531272265534, 11.49999999999999645 ) ) ;
#39614=CARTESIAN_POINT ( 'NONE',  ( -40.62287095715005592, -29.50247984919015209, -1.443849546365060466 ) ) ;
#39615=AXIS2_PLACEMENT_3D ( 'NONE', #28970, #21344, #90374 ) ;
#39617=CARTESIAN_POINT ( 'NONE',  ( -12.43717309395686499, -17.31322327496724611, 11.49999999999998934 ) ) ;
#39618=CARTESIAN_POINT ( 'NONE',  ( -98.59947919455895260, -23.48786465467241058, 11.44779295918254114 ) ) ;
#39619=CARTESIAN_POINT ( 'NONE',  ( -46.52287095715006160, -24.64965694238406613, 8.947790433994203596 ) ) ;
#39620=CARTESIAN_POINT ( 'NONE',  ( -64.62365174556643410, -24.66019654487199730, 8.947790411086115725 ) ) ;
#39621=CARTESIAN_POINT ( 'NONE',  ( -71.31679247717998749, -25.22594453560301631, 6.517383687127669134 ) ) ;
#39622=CARTESIAN_POINT ( 'NONE',  ( -18.95691745938505335, -12.16397891629814865, -1.500000000000002220 ) ) ;
#39623=B_SPLINE_CURVE_WITH_KNOTS ( 'NONE', 3,
 ( #5665, #68074, #36616, #21373, #52349, #83782, #75660, #45238 ),
 .UNSPECIFIED., .F., .F.,
 ( 4, 2, 2, 4 ),
 ( -0.001240666984356058331, -0.0002401179793396601269, 0.0007604310256767380771, 0.002761529035709534702 ),
 .UNSPECIFIED. ) ;
#39626=CARTESIAN_POINT ( 'NONE',  ( -51.52764846858840997, -25.25773520710183817, 6.187572766161611781 ) ) ;
#39628=CARTESIAN_POINT ( 'NONE',  ( 19.69511366699831001, -0.05742560045514189665, 11.49999999999999645 ) ) ;
#39629=CARTESIAN_POINT ( 'NONE',  ( -109.5228709571500616, -24.64965694238408034, 8.947790433994192938 ) ) ;
#39630=B_SPLINE_CURVE_WITH_KNOTS ( 'NONE', 3,
 ( #25940, #65037, #49298, #2618, #4112, #95949 ),
 .UNSPECIFIED., .F., .F.,
 ( 4, 2, 4 ),
 ( 6.384118678611710879E-06, 0.001386860460828373467, 0.002767336802978134953 ),
 .UNSPECIFIED. ) ;
#39632=ORIENTED_EDGE ( 'NONE', *, *, #45911, .T. ) ;
#39633=CARTESIAN_POINT ( 'NONE',  ( -99.62355589612486995, -24.65952944569304961, 1.056160979905703901 ) ) ;
#39637=CARTESIAN_POINT ( 'NONE',  ( 11.81298147481671279, -15.83112273922526470, 11.49999999999998934 ) ) ;
#39643=EDGE_LOOP ( 'NONE', ( #35126, #22447, #47104, #31863 ) ) ;
#39647=LINE ( 'NONE', #32038, #88193 ) ;
#39648=CARTESIAN_POINT ( 'NONE',  ( -85.58953762381671027, -23.48783264082478794, -1.443836473390063713 ) ) ;
#39649=LINE ( 'NONE', #62498, #55406 ) ;
#39651=CARTESIAN_POINT ( 'NONE',  ( -6.099057486122481997, -19.05896565686126110, 11.49999999999998934 ) ) ;
#39657=CARTESIAN_POINT ( 'NONE',  ( -109.3608459871604026, -25.18430332269756633, 4.114985099319373951 ) ) ;
#39658=CARTESIAN_POINT ( 'NONE',  ( -35.59336923871764924, -24.40034930558991277, 0.3402023900116170063 ) ) ;
#39659=CARTESIAN_POINT ( 'NONE',  ( -28.62287095715005236, -23.58365284793268302, 11.05752274016301584 ) ) ;
#39660=CARTESIAN_POINT ( 'NONE',  ( -76.62287095715007013, -29.50250243563736774, 8.947779886222141599 ) ) ;
#39661=DIRECTION ( 'NONE',  ( -3.773278334453079618E-23, 0.9999999999976377785, 2.173523156925978705E-06 ) ) ;
#39663=CARTESIAN_POINT ( 'NONE',  ( -63.62287095715001328, -23.73934037231756378, 11.05740245334329153 ) ) ;
#39665=CARTESIAN_POINT ( 'NONE',  ( -50.40445135320380388, -25.18492896333868103, 3.293943116708552221 ) ) ;
#39666=ORIENTED_EDGE ( 'NONE', *, *, #41191, .T. ) ;
#39667=CARTESIAN_POINT ( 'NONE',  ( 6.837353022973060135, 19.10023500134885310, -1.500000000000002220 ) ) ;
#39669=EDGE_CURVE ( 'NONE', #9517, #44155, #80064, .T. ) ;
#39670=CARTESIAN_POINT ( 'NONE',  ( -59.48966412625335920, -24.66019654487199730, 8.947790411086124607 ) ) ;
#39671=EDGE_CURVE ( 'NONE', #19988, #21619, #15888, .T. ) ;
#39673=FACE_OUTER_BOUND ( 'NONE', #60486, .T. ) ;
#39674=CARTESIAN_POINT ( 'NONE',  ( 8.007726535620864894, 18.53121347637897287, -1.500000000000002220 ) ) ;
#39675=CARTESIAN_POINT ( 'NONE',  ( -18.40674794014382698, -10.35651468716735657, 11.49999999999999645 ) ) ;
#39676=EDGE_CURVE ( 'NONE', #32756, #37373, #70356, .T. ) ;
#39678=CARTESIAN_POINT ( 'NONE',  ( -21.04927197579530329, -6.814310187297170529, -1.500000000000002220 ) ) ;
#39679=CARTESIAN_POINT ( 'NONE',  ( -17.31529204923715071, 11.11782870402162260, -1.500000000000002220 ) ) ;
#39682=FACE_OUTER_BOUND ( 'NONE', #75803, .T. ) ;
#39683=ORIENTED_EDGE ( 'NONE', *, *, #3859, .F. ) ;
#39684=LINE ( 'NONE', #76728, #17137 ) ;
#39685=CARTESIAN_POINT ( 'NONE',  ( -110.6228709571500559, -23.85229601348996908, 10.88205029486208808 ) ) ;
#39687=ORIENTED_EDGE ( 'NONE', *, *, #26422, .T. ) ;
#39688=VERTEX_POINT ( 'NONE', #67468 ) ;
#39689=CARTESIAN_POINT ( 'NONE',  ( -110.7007163551309361, -25.12832023213188037, 2.875934489414091466 ) ) ;
#39691=CARTESIAN_POINT ( 'NONE',  ( -68.55392418078596961, -23.96169478059712787, 10.65365249895718414 ) ) ;
#39692=CARTESIAN_POINT ( 'NONE',  ( -20.55277978778089576, -2.218614319624547360, -1.500000000000002220 ) ) ;
#39693=ADVANCED_FACE ( 'NONE', ( #76061 ), #6560, .T. ) ;
#39694=CARTESIAN_POINT ( 'NONE',  ( 19.61570337458852364, 9.273991169892711994, 11.49999999999999645 ) ) ;
#39695=VERTEX_POINT ( 'NONE', #37509 ) ;
#39698=CARTESIAN_POINT ( 'NONE',  ( 3.752539591237177508, -22.04708138622333635, -1.500000000000002220 ) ) ;
#39699=CARTESIAN_POINT ( 'NONE',  ( -79.34687923781920915, -25.12205563760222304, 5.960409599525325675 ) ) ;
#39700=CARTESIAN_POINT ( 'NONE',  ( -84.50376481693795938, -24.51314013834316441, 0.6176544820404183955 ) ) ;
#39701=VERTEX_POINT ( 'NONE', #59350 ) ;
#39702=CARTESIAN_POINT ( 'NONE',  ( -118.8947150340837311, -25.34770440169397787, 6.200377556431414305 ) ) ;
#39703=CARTESIAN_POINT ( 'NONE',  ( -76.62287095715005592, -24.33927499327854704, 9.819080762295818943 ) ) ;
#39705=VECTOR ( 'NONE', #51284, 1000.000000000000114 ) ;
#39706=CARTESIAN_POINT ( 'NONE',  ( -70.62287095715004170, -23.48783264082478084, -1.443836473390067265 ) ) ;
#39709=CARTESIAN_POINT ( 'NONE',  ( -109.5906666788849009, -24.15620529776628800, 10.23563542870660115 ) ) ;
#39710=CARTESIAN_POINT ( 'NONE',  ( -14.79452276021403634, 15.15755283273500531, -1.500000000000002220 ) ) ;
#39711=EDGE_CURVE ( 'NONE', #55090, #90388, #30390, .T. ) ;
#39712=EDGE_LOOP ( 'NONE', ( #76844, #81735, #67010, #49442 ) ) ;
#39713=CARTESIAN_POINT ( 'NONE',  ( -50.60042094805579183, -24.15503026093913164, -0.2815557561904566963 ) ) ;
#39714=CARTESIAN_POINT ( 'NONE',  ( -16.21501377034323710, -14.60173171477820198, -1.500000000000002220 ) ) ;
#39716=CARTESIAN_POINT ( 'NONE',  ( -52.62287095715005592, -29.50250786944525672, 11.44777988621624054 ) ) ;
#39718=CARTESIAN_POINT ( 'NONE',  ( -5.167225684058948332, 21.16526716281445530, -1.500000000000002220 ) ) ;
#39722=CARTESIAN_POINT ( 'NONE',  ( -85.51575146014167217, -23.85049219812685450, 10.88485053497527133 ) ) ;
#39724=VERTEX_POINT ( 'NONE', #53246 ) ;
#39727=ADVANCED_FACE ( 'NONE', ( #82679 ), #37012, .T. ) ;
#39732=CARTESIAN_POINT ( 'NONE',  ( -113.6228709571500417, -24.51283580621365132, 0.6167428607019899145 ) ) ;
#39733=CARTESIAN_POINT ( 'NONE',  ( -19.98547761299008130, 7.154247560337752887, -1.500000000000002220 ) ) ;
#39734=CARTESIAN_POINT ( 'NONE',  ( -121.6228709571500417, -24.64898659630368627, 1.056161002820833028 ) ) ;
#39735=CARTESIAN_POINT ( 'NONE',  ( -30.61048516611183601, -24.43626637953622804, 0.1835287498755953373 ) ) ;
#39736=CARTESIAN_POINT ( 'NONE',  ( -38.62287095715005592, -29.50247984919015209, -1.443849546365060466 ) ) ;
#39738=CARTESIAN_POINT ( 'NONE',  ( 2.844571010020486845, -19.19604305453586690, 11.49999999999998934 ) ) ;
#39739=CARTESIAN_POINT ( 'NONE',  ( -41.89562512939934891, -25.03707806782366418, 7.590868867492675420 ) ) ;
#39740=EDGE_LOOP ( 'NONE', ( #74011, #87375, #90015, #60433 ) ) ;
#39741=CARTESIAN_POINT ( 'NONE',  ( -1.849579639615634097, -19.42000222497389927, 11.49999999999999645 ) ) ;
#39742=CARTESIAN_POINT ( 'NONE',  ( -42.52287095715005449, -24.50321055353804311, 9.387540953477529371 ) ) ;
#39743=CARTESIAN_POINT ( 'NONE',  ( -79.57618923056713811, -25.19206956779440887, 6.661130867067107886 ) ) ;
#39744=ORIENTED_EDGE ( 'NONE', *, *, #45458, .F. ) ;
#39747=CARTESIAN_POINT ( 'NONE',  ( -103.5895376238167387, -23.47593901973091235, -1.443836447539001089 ) ) ;
#39748=CARTESIAN_POINT ( 'NONE',  ( -93.51533444581417598, -23.96169478059713853, 10.65365249895717348 ) ) ;
#39749=CARTESIAN_POINT ( 'NONE',  ( -3.719764837209879271, -19.30396570740023421, -1.500000000000002220 ) ) ;
#39750=CARTESIAN_POINT ( 'NONE',  ( -41.15947890742572923, -25.31583714713193700, 4.822226109655245452 ) ) ;
#39751=ORIENTED_EDGE ( 'NONE', *, *, #70513, .F. ) ;
#39753=CARTESIAN_POINT ( 'NONE',  ( 21.54666897473465070, 1.519730039111064412, -1.500000000000002220 ) ) ;
#39756=CARTESIAN_POINT ( 'NONE',  ( -13.34915495237762251, 18.83725853537101358, -1.500000000000002220 ) ) ;
#39758=CARTESIAN_POINT ( 'NONE',  ( -92.22287095715005023, -23.47593901973090169, -1.443836447538996870 ) ) ;
#39759=CARTESIAN_POINT ( 'NONE',  ( -130.5728709571500588, -23.47593901973090524, -1.443836447538995982 ) ) ;
#39760=DIRECTION ( 'NONE',  ( 3.773278334444166432E-23, -1.000000000000000000, 0.000000000000000000 ) ) ;
#39762=CARTESIAN_POINT ( 'NONE',  ( -111.6658724870577117, -25.29824007310582701, 3.734855809897266621 ) ) ;
#39763=CARTESIAN_POINT ( 'NONE',  ( -98.52287095715009002, -23.72747288104470798, -1.053458166803226126 ) ) ;
#39764=FACE_OUTER_BOUND ( 'NONE', #24430, .T. ) ;
#39765=CARTESIAN_POINT ( 'NONE',  ( 2.927915493035635031, 19.71835975189664936, -1.500000000000002220 ) ) ;
#39766=CARTESIAN_POINT ( 'NONE',  ( -75.54453366976977691, -24.52399227489127043, 9.353111116836526406 ) ) ;
#39767=CARTESIAN_POINT ( 'NONE',  ( -17.59554656748941071, 9.132484154288260214, -1.500000000000002220 ) ) ;
#39768=ORIENTED_EDGE ( 'NONE', *, *, #28886, .F. ) ;
#39769=CARTESIAN_POINT ( 'NONE',  ( -56.55997151016966029, -23.73766607897670511, -1.055555164236459342 ) ) ;
#39770=CARTESIAN_POINT ( 'NONE',  ( -39.04303308397305727, -25.10925892954523064, 4.215217319642836635 ) ) ;
#39772=CARTESIAN_POINT ( 'NONE',  ( -18.43438512255917772, -9.567967903218889347, 11.49999999999999645 ) ) ;
#39773=CARTESIAN_POINT ( 'NONE',  ( -100.6814946224345846, -29.50249328176098729, 4.736241424693623081 ) ) ;
#39775=CARTESIAN_POINT ( 'NONE',  ( -106.5908035580171287, -24.15543982623907127, -0.2315651400026576268 ) ) ;
#39776=CARTESIAN_POINT ( 'NONE',  ( -10.92962168092244823, 19.99562239114850826, 11.49999999999999645 ) ) ;
#39778=ORIENTED_EDGE ( 'NONE', *, *, #20418, .T. ) ;
#39779=EDGE_CURVE ( 'NONE', #52807, #20892, #38701, .T. ) ;
#39781=CARTESIAN_POINT ( 'NONE',  ( -70.26171360675115807, -25.12330951983202709, 7.099796482853127699 ) ) ;
#39782=EDGE_CURVE ( 'NONE', #62158, #89034, #3686, .T. ) ;
#39785=CARTESIAN_POINT ( 'NONE',  ( -19.33604739795523741, 5.927148246271303655, 11.49999999999998934 ) ) ;
#39786=DIRECTION ( 'NONE',  ( -0.000000000000000000, 2.173523156925979552E-06, -0.9999999999976378895 ) ) ;
#39788=EDGE_CURVE ( 'NONE', #50965, #57581, #7558, .T. ) ;
#39789=CARTESIAN_POINT ( 'NONE',  ( -110.5228709571500048, -24.15516710230294350, 10.28746687063725140 ) ) ;
#39790=ADVANCED_FACE ( 'NONE', ( #86182 ), #94288, .F. ) ;
#39792=EDGE_CURVE ( 'NONE', #21561, #28755, #27939, .T. ) ;
#39793=B_SPLINE_CURVE_WITH_KNOTS ( 'NONE', 3,
 ( #69348, #44519, #37900, #91673, #5450, #67362 ),
 .UNSPECIFIED., .F., .F.,
 ( 4, 2, 4 ),
 ( 6.391158118966174708E-06, 0.001387004593080782677, 0.002767618028042598960 ),
 .UNSPECIFIED. ) ;
#39795=CARTESIAN_POINT ( 'NONE',  ( -125.5228709571500616, -23.47593901973090524, -1.443836447538996204 ) ) ;
#39796=CARTESIAN_POINT ( 'NONE',  ( 7.457602374657920308, -21.66695214233757838, -1.500000000000002220 ) ) ;
#39797=CARTESIAN_POINT ( 'NONE',  ( -50.67443072449054853, -25.18439655831317836, 3.321634571026201854 ) ) ;
#39798=CARTESIAN_POINT ( 'NONE',  ( -18.23705311251027794, 8.147635122911419003, -1.500000000000002220 ) ) ;
#39800=CARTESIAN_POINT ( 'NONE',  ( 5.581485548573628996, 20.18083795961418403, 11.49999999999999645 ) ) ;
#39801=VERTEX_POINT ( 'NONE', #1962 ) ;
#39803=CARTESIAN_POINT ( 'NONE',  ( -89.52287095715003318, -23.48783264083374789, -1.443836473376144180 ) ) ;
#39804=CARTESIAN_POINT ( 'NONE',  ( -69.53040046975404209, -25.24754292466213101, 5.066170387013165133 ) ) ;
#39805=CARTESIAN_POINT ( 'NONE',  ( -20.26759042640731323, -8.618136523154847239, 11.49999999999998934 ) ) ;
#39807=VERTEX_POINT ( 'NONE', #92784 ) ;
#39808=CARTESIAN_POINT ( 'NONE',  ( -118.5228709571500474, -23.73934037231757443, 11.05740245334327909 ) ) ;
#39809=CARTESIAN_POINT ( 'NONE',  ( -122.6228709571500417, -23.47596703998600631, 11.44779298504227860 ) ) ;
#39810=B_SPLINE_CURVE_WITH_KNOTS ( 'NONE', 3,
 ( #25303, #9081, #86701, #69980 ),
 .UNSPECIFIED., .F., .F.,
 ( 4, 4 ),
 ( 0.000000000000000000, 9.999999999998897304E-05 ),
 .UNSPECIFIED. ) ;
#39813=VERTEX_POINT ( 'NONE', #85178 ) ;
#39814=EDGE_LOOP ( 'NONE', ( #32955, #51053, #63045, #99999 ) ) ;
#39815=CARTESIAN_POINT ( 'NONE',  ( -101.3738023147422638, -25.26303730729093999, 3.986250639247583827 ) ) ;
#39816=CARTESIAN_POINT ( 'NONE',  ( -100.5578068411443837, -25.27404630875477665, 2.834635289093140109 ) ) ;
#39818=CARTESIAN_POINT ( 'NONE',  ( 20.25987197511681259, 2.754759976156288204, -1.500000000000002220 ) ) ;
#39820=ORIENTED_EDGE ( 'NONE', *, *, #95820, .T. ) ;
#39822=CARTESIAN_POINT ( 'NONE',  ( -33.62287095715005592, -23.96177878511307568, 10.65340807706330573 ) ) ;
#39824=CARTESIAN_POINT ( 'NONE',  ( 22.20884612314100792, -2.053178116692622623, -1.500000000000002220 ) ) ;
#39827=EDGE_CURVE ( 'NONE', #82876, #50012, #81130, .T. ) ;
#39828=VERTEX_POINT ( 'NONE', #80071 ) ;
#39829=CARTESIAN_POINT ( 'NONE',  ( -27.89347163551325792, -24.62105267781937457, 1.634524268193336072 ) ) ;
#39830=CARTESIAN_POINT ( 'NONE',  ( -118.5228709571500900, -24.33832256527048798, 0.1851278514138662290 ) ) ;
#39832=CARTESIAN_POINT ( 'NONE',  ( -16.21995886604411297, 13.06735728859114509, -1.500000000000002220 ) ) ;
#39833=ORIENTED_EDGE ( 'NONE', *, *, #73694, .F. ) ;
#39834=CARTESIAN_POINT ( 'NONE',  ( -79.52287095715006160, -23.48786465467241058, 11.44779295918254469 ) ) ;
#39836=ORIENTED_EDGE ( 'NONE', *, *, #54445, .T. ) ;
#39837=ORIENTED_EDGE ( 'NONE', *, *, #54819, .F. ) ;
#39839=CARTESIAN_POINT ( 'NONE',  ( -20.73700405699343463, 3.470425206167693233, -1.500000000000002220 ) ) ;
#39841=CARTESIAN_POINT ( 'NONE',  ( -37.52287095715006870, -24.64965694238406613, 8.947790433994205372 ) ) ;
#39844=CARTESIAN_POINT ( 'NONE',  ( -101.8248201165894073, -25.25419362369936849, 6.680466494418182855 ) ) ;
#39845=CARTESIAN_POINT ( 'NONE',  ( -60.62287095715004881, -24.51254535404256174, 9.355368623467651190 ) ) ;
#39846=LINE ( 'NONE', #79406, #33566 ) ;
#39847=CARTESIAN_POINT ( 'NONE',  ( 13.49617185221842952, 17.62045156095830123, 11.49999999999999645 ) ) ;
#39849=CARTESIAN_POINT ( 'NONE',  ( -39.52287095715006870, -29.50250786944525672, 11.44777988621624232 ) ) ;
#39850=CARTESIAN_POINT ( 'NONE',  ( -38.62287095715005592, -23.73907113216990794, -1.053371485793235918 ) ) ;
#39852=CARTESIAN_POINT ( 'NONE',  ( -16.08347380570801377, -15.98036338121420030, 11.49999999999998934 ) ) ;
#39853=ADVANCED_FACE ( 'NONE', ( #73462 ), #50129, .F. ) ;
#39854=DIRECTION ( 'NONE',  ( -3.773278334453079030E-23, 0.9999999999976377785, 2.173523156925979128E-06 ) ) ;
#39855=VERTEX_POINT ( 'NONE', #41514 ) ;
#39856=ORIENTED_EDGE ( 'NONE', *, *, #84822, .F. ) ;
#39858=ADVANCED_FACE ( 'NONE', ( #64882 ), #77555, .T. ) ;
#39859=B_SPLINE_CURVE_WITH_KNOTS ( 'NONE', 3,
 ( #84016, #84517, #77390, #15996, #99235, #39341, #46460, #62198 ),
 .UNSPECIFIED., .F., .F.,
 ( 4, 2, 2, 4 ),
 ( 0.000000000000000000, 0.002001079623178221491, 0.003001619434767333755, 0.004002159246356446452 ),
 .UNSPECIFIED. ) ;
#39860=VECTOR ( 'NONE', #57301, 1000.000000000000114 ) ;
#39861=CARTESIAN_POINT ( 'NONE',  ( 18.53703574427524359, 7.882278514257341051, 11.49999999999998934 ) ) ;
#39862=CARTESIAN_POINT ( 'NONE',  ( -80.62287095715001328, -24.92579138211019085, 1.929029949965667123 ) ) ;
#39865=CARTESIAN_POINT ( 'NONE',  ( -39.04303308397305727, -29.50249214928227914, 4.215207770848699020 ) ) ;
#39866=CARTESIAN_POINT ( 'NONE',  ( -12.73782554413503654, -18.45060914899308457, -1.500000000000002220 ) ) ;
#39868=ADVANCED_FACE ( 'NONE', ( #56257 ), #81073, .F. ) ;
#39869=AXIS2_PLACEMENT_3D ( 'NONE', #55373, #93914, #70083 ) ;
#39871=VERTEX_POINT ( 'NONE', #79569 ) ;
#39872=CARTESIAN_POINT ( 'NONE',  ( -112.5905324053159262, -24.15620529776628445, 10.23563542870659582 ) ) ;
#39874=DIRECTION ( 'NONE',  ( 0.000000000000000000, 0.9999999999976377785, 2.173523156925979975E-06 ) ) ;
#39875=CARTESIAN_POINT ( 'NONE',  ( -122.6228709571500417, -29.50248528299804818, 1.056150453629045360 ) ) ;
#39876=CARTESIAN_POINT ( 'NONE',  ( -97.25162849029662482, -24.37807914296825729, 0.3010598746230577216 ) ) ;
#39877=CARTESIAN_POINT ( 'NONE',  ( -0.9579564967699066846, 19.55851204243107233, -1.500000000000002220 ) ) ;
#39879=VERTEX_POINT ( 'NONE', #10058 ) ;
#39880=CARTESIAN_POINT ( 'NONE',  ( 21.44729954461699251, -1.519088741117538000, -1.500000000000002220 ) ) ;
#39881=CARTESIAN_POINT ( 'NONE',  ( -31.62287095715005236, -29.50250243563736774, 8.947779886222150481 ) ) ;
#39884=CARTESIAN_POINT ( 'NONE',  ( -80.62287095715004170, -24.82576562982391977, 8.398263435472973271 ) ) ;
#39885=CARTESIAN_POINT ( 'NONE',  ( -9.675568039816649701, -20.77828039667204862, -1.500000000000002220 ) ) ;
#39887=CARTESIAN_POINT ( 'NONE',  ( -96.51589611984518058, -23.96169478059713498, 10.65365249895717881 ) ) ;
#39889=CARTESIAN_POINT ( 'NONE',  ( 12.62869658624171976, -15.57725692549414376, 11.49999999999999645 ) ) ;
#39890=CARTESIAN_POINT ( 'NONE',  ( -79.79643364552497076, -25.31594337936764205, 4.606720419479115591 ) ) ;
#39894=VERTEX_POINT ( 'NONE', #71974 ) ;
#39895=CARTESIAN_POINT ( 'NONE',  ( -83.62287095715005592, -29.50250243563736774, 8.947779886222141599 ) ) ;
#39896=CARTESIAN_POINT ( 'NONE',  ( 21.40858030128615397, -3.853468400179685727, 11.49999999999998934 ) ) ;
#39897=LINE ( 'NONE', #38896, #90126 ) ;
#39898=CARTESIAN_POINT ( 'NONE',  ( -0.7274468246531539117, 19.66889477801398911, -1.500000000000002220 ) ) ;
#39900=DIRECTION ( 'NONE',  ( 3.773278334444166432E-23, -1.000000000000000000, 0.000000000000000000 ) ) ;
#39901=CARTESIAN_POINT ( 'NONE',  ( -104.5895376238167245, -23.48786465467241413, 11.44779295918254114 ) ) ;
#39903=CARTESIAN_POINT ( 'NONE',  ( -91.54630222961577601, -24.51419770103159124, 9.386484678747176957 ) ) ;
#39905=CARTESIAN_POINT ( 'NONE',  ( -16.28974412851428255, -12.55652860423730388, 11.49999999999999645 ) ) ;
#39907=CARTESIAN_POINT ( 'NONE',  ( -120.5208179319231476, -23.85016227208581441, -0.8807180028928250914 ) ) ;
#39908=CARTESIAN_POINT ( 'NONE',  ( -21.41681981171885951, -7.298096547245328303, 11.49999999999999645 ) ) ;
#39910=EDGE_CURVE ( 'NONE', #60838, #55188, #2455, .T. ) ;
#39911=CARTESIAN_POINT ( 'NONE',  ( -99.82150581108260212, -25.26387405423741583, 4.513512927829998134 ) ) ;
#39912=LINE ( 'NONE', #71879, #59144 ) ;
#39913=CARTESIAN_POINT ( 'NONE',  ( -125.5204572650066552, -24.40133493613050675, 9.663955038902798833 ) ) ;
#39914=EDGE_CURVE ( 'NONE', #27902, #38599, #13363, .T. ) ;
#39916=EDGE_CURVE ( 'NONE', #21576, #65701, #25782, .T. ) ;
#39917=CARTESIAN_POINT ( 'NONE',  ( -33.62287095715007013, -23.94994826722565762, -0.6494450866342740269 ) ) ;
#39919=PLANE ( 'NONE',  #36614 ) ;
#39921=VECTOR ( 'NONE', #28403, 1000.000000000000114 ) ;
#39923=CARTESIAN_POINT ( 'NONE',  ( -80.09072421954219578, -25.26749884311348282, 5.004106523481387292 ) ) ;
#39924=CARTESIAN_POINT ( 'NONE',  ( -19.65108876255925807, -11.61119296138784662, -1.500000000000002220 ) ) ;
#39926=CARTESIAN_POINT ( 'NONE',  ( -96.63021477443740537, -24.15543982623907482, -0.2315651400026596807 ) ) ;
#39927=CARTESIAN_POINT ( 'NONE',  ( -63.62744501956971277, -24.51419770103158058, 9.386484678747173405 ) ) ;
#39928=CARTESIAN_POINT ( 'NONE',  ( -15.60622653811170402, 16.18669697583415967, 11.49999999999999645 ) ) ;
#39931=CARTESIAN_POINT ( 'NONE',  ( 21.92589416912191069, -1.073809401359021143, -1.500000000000002220 ) ) ;
#39934=CARTESIAN_POINT ( 'NONE',  ( -44.58706610318112951, -24.35071581493542681, 9.817618358456025263 ) ) ;
#39936=ORIENTED_EDGE ( 'NONE', *, *, #23551, .F. ) ;
#39937=PLANE ( 'NONE',  #617 ) ;
#39938=LINE ( 'NONE', #70900, #56616 ) ;
#39939=VERTEX_POINT ( 'NONE', #74452 ) ;
#39941=CARTESIAN_POINT ( 'NONE',  ( -12.74120943341865342, -16.01528480738631899, 11.49999999999998934 ) ) ;
#39942=VERTEX_POINT ( 'NONE', #97292 ) ;
#39944=VERTEX_POINT ( 'NONE', #59740 ) ;
#39946=ORIENTED_EDGE ( 'NONE', *, *, #98079, .F. ) ;
#39947=CARTESIAN_POINT ( 'NONE',  ( 10.36671515591691950, -20.60271000134967068, -1.500000000000002220 ) ) ;
#39949=CARTESIAN_POINT ( 'NONE',  ( -20.26613141553852060, -1.498020344548873561, -1.500000000000002220 ) ) ;
#39950=ORIENTED_EDGE ( 'NONE', *, *, #4546, .F. ) ;
#39952=CARTESIAN_POINT ( 'NONE',  ( -40.62287095715004170, -24.99156045073392463, 7.747789690856161648 ) ) ;
#39954=CARTESIAN_POINT ( 'NONE',  ( -99.52287095715006160, -29.50250243563736774, 8.947779886222138046 ) ) ;
#39956=CARTESIAN_POINT ( 'NONE',  ( -20.40864349294084334, -6.676163967499375573, 11.49999999999999645 ) ) ;
#39958=CARTESIAN_POINT ( 'NONE',  ( -79.62287095715007013, -24.66019654487199375, 8.947790411086128159 ) ) ;
#39959=CARTESIAN_POINT ( 'NONE',  ( -93.52287095715007581, -23.95044443724993144, 10.65354141964648882 ) ) ;
#39961=CARTESIAN_POINT ( 'NONE',  ( 19.63682106917175929, 6.691539877478525966, -1.500000000000002220 ) ) ;
#39962=VERTEX_POINT ( 'NONE', #66860 ) ;
#39963=CARTESIAN_POINT ( 'NONE',  ( -125.5541640623637250, -24.92564183028979485, 1.928384488918254425 ) ) ;
#39965=CARTESIAN_POINT ( 'NONE',  ( -111.5512703140825863, -24.51419770103157703, 9.386484678747162747 ) ) ;
#39967=ORIENTED_EDGE ( 'NONE', *, *, #99711, .T. ) ;
#39968=ORIENTED_EDGE ( 'NONE', *, *, #65724, .F. ) ;
#39969=CARTESIAN_POINT ( 'NONE',  ( -40.52287095715007581, -24.83602698348160231, 1.605859176311261960 ) ) ;
#39970=CARTESIAN_POINT ( 'NONE',  ( -42.53972667629340521, -24.35071581493542681, 9.817618358456037697 ) ) ;
#39971=CARTESIAN_POINT ( 'NONE',  ( -78.52287095715006160, -24.64898659630367916, 1.056161002820826145 ) ) ;
#39972=CARTESIAN_POINT ( 'NONE',  ( -10.13730173486854369, -19.54584281717935568, 11.49999999999999645 ) ) ;
#39973=CARTESIAN_POINT ( 'NONE',  ( -89.59823446461851404, -23.73791477778911840, 11.05961554403170233 ) ) ;
#39974=CARTESIAN_POINT ( 'NONE',  ( -16.68516988606489448, 15.22057433622007316, -1.500000000000002220 ) ) ;
#39975=EDGE_CURVE ( 'NONE', #98189, #40469, #8533, .T. ) ;
#39976=VECTOR ( 'NONE', #14104, 1000.000000000000114 ) ;
#39977=CARTESIAN_POINT ( 'NONE',  ( -1.027814097295878693, -20.98676634966329146, -1.500000000000002220 ) ) ;
#39978=PLANE ( 'NONE',  #42558 ) ;
#39979=VERTEX_POINT ( 'NONE', #74932 ) ;
#39980=B_SPLINE_CURVE_WITH_KNOTS ( 'NONE', 3,
 ( #26160, #19043, #42414, #78934, #72348, #11435, #96669, #88568, #56130, #2844, #58129, #94668, #18048, #89066 ),
 .UNSPECIFIED., .F., .F.,
 ( 4, 2, 2, 2, 2, 2, 4 ),
 ( 0.000000000000000000, 0.0002404508101542971810, 0.0004809016203085943620, 0.0009618032406171489338, 0.001442704860925703722, 0.001683155671079981062, 0.001923606481234258186 ),
 .UNSPECIFIED. ) ;
#39983=DIRECTION ( 'NONE',  ( 0.000000000000000000, -0.9999999999976377785, -2.173523156925979128E-06 ) ) ;
#39985=EDGE_CURVE ( 'NONE', #25180, #41495, #49703, .T. ) ;
#39986=CARTESIAN_POINT ( 'NONE',  ( -90.62287095715005592, -24.91570333823099759, 8.075032458375558164 ) ) ;
#39987=VERTEX_POINT ( 'NONE', #22143 ) ;
#39988=CARTESIAN_POINT ( 'NONE',  ( 21.14167878903947084, -0.5806874866175276706, -1.500000000000002220 ) ) ;
#39989=CARTESIAN_POINT ( 'NONE',  ( -117.5228709571500758, -23.47593901973090524, -1.443836447538996204 ) ) ;
#39990=CARTESIAN_POINT ( 'NONE',  ( -51.32936205048392964, -25.03148689476321564, 7.321356269641313474 ) ) ;
#39991=CARTESIAN_POINT ( 'NONE',  ( -121.5901305642217807, -24.15543982623907482, -0.2315651400026574047 ) ) ;
#39992=CARTESIAN_POINT ( 'NONE',  ( -51.92287095715005307, -23.47593901973090169, -1.443836447538997758 ) ) ;
#39993=CARTESIAN_POINT ( 'NONE',  ( -127.5228709571500616, -23.96177878511310411, 10.65340807706329684 ) ) ;
#39994=CARTESIAN_POINT ( 'NONE',  ( 21.93305185196877360, -3.456643806985262302, -1.500000000000002220 ) ) ;
#39996=VERTEX_POINT ( 'NONE', #36389 ) ;
#39997=CARTESIAN_POINT ( 'NONE',  ( -51.04357394935764347, -25.24859992533754038, 4.940878074475977044 ) ) ;
#39998=CARTESIAN_POINT ( 'NONE',  ( -37.59389932947581059, -24.15543982623907127, -0.2315651400026566831 ) ) ;
#40001=CARTESIAN_POINT ( 'NONE',  ( -75.62287095715005592, -23.47593901973091235, -1.443836447539004642 ) ) ;
#40002=CARTESIAN_POINT ( 'NONE',  ( -100.5192865818111159, -25.11060891163327469, 2.833917758948478305 ) ) ;
#40003=CARTESIAN_POINT ( 'NONE',  ( 18.45204572605500104, 6.281640480902235701, 11.49999999999998934 ) ) ;
#40004=CARTESIAN_POINT ( 'NONE',  ( 9.091334071971768793, -19.38302982324925239, -1.500000000000002220 ) ) ;
#40005=CARTESIAN_POINT ( 'NONE',  ( -85.52287095715006160, -24.14406661686761169, 10.28769366194077861 ) ) ;
#40006=PLANE ( 'NONE',  #93314 ) ;
#40007=CARTESIAN_POINT ( 'NONE',  ( -51.64512162636743398, -23.96119346886880663, -0.6495511937832119109 ) ) ;
#40008=DIRECTION ( 'NONE',  ( -1.000000000000000000, -3.773278334444166432E-23, -8.201307841325785021E-29 ) ) ;
#40009=CARTESIAN_POINT ( 'NONE',  ( 15.30562342774392093, -16.77826389816909725, -1.500000000000002220 ) ) ;
#40011=AXIS2_PLACEMENT_3D ( 'NONE', #89011, #42847, #50447 ) ;
#40012=CARTESIAN_POINT ( 'NONE',  ( -32.62287095715004881, -23.48786465467240347, 11.44779295918255535 ) ) ;
#40014=CARTESIAN_POINT ( 'NONE',  ( 13.99221305778824487, -14.08248706038611964, 11.49999999999999645 ) ) ;
#40015=CARTESIAN_POINT ( 'NONE',  ( -123.6234902540211493, -24.66019654487200441, 8.947790411086106843 ) ) ;
#40016=VECTOR ( 'NONE', #27983, 1000.000000000000114 ) ;
#40017=B_SPLINE_CURVE_WITH_KNOTS ( 'NONE', 3,
 ( #40488, #48614, #94260, #86651, #24743, #95269 ),
 .UNSPECIFIED., .F., .F.,
 ( 4, 2, 4 ),
 ( 0.000000000000000000, 0.001380764517854761713, 0.002761529035709523426 ),
 .UNSPECIFIED. ) ;
#40018=CARTESIAN_POINT ( 'NONE',  ( -54.52287095715006870, -23.47596703998600631, 11.44779298504229104 ) ) ;
#40019=B_SPLINE_CURVE_WITH_KNOTS ( 'NONE', 3,
 ( #48084, #55704, #79010, #9508 ),
 .UNSPECIFIED., .F., .F.,
 ( 4, 4 ),
 ( 0.000000000000000000, 9.999999999998900014E-05 ),
 .UNSPECIFIED. ) ;
#40024=CARTESIAN_POINT ( 'NONE',  ( -117.5895376238167387, -24.66019654487199730, 8.947790411086122830 ) ) ;
#40025=CARTESIAN_POINT ( 'NONE',  ( -21.63489631200954122, -1.325961216813365429, -1.500000000000002220 ) ) ;
#40027=CARTESIAN_POINT ( 'NONE',  ( 0.2958748881272694198, 19.47992435465491212, -1.500000000000002220 ) ) ;
#40028=VECTOR ( 'NONE', #76659, 1000.000000000000114 ) ;
#40029=CARTESIAN_POINT ( 'NONE',  ( -55.53421905444260176, -24.73531770709095312, 8.716586749053510275 ) ) ;
#40030=ADVANCED_FACE ( 'NONE', ( #82557 ), #60243, .F. ) ;
#40031=VERTEX_POINT ( 'NONE', #59233 ) ;
#40032=CARTESIAN_POINT ( 'NONE',  ( -11.21218820807429140, -16.99972530465495169, 11.49999999999999645 ) ) ;
#40035=ORIENTED_EDGE ( 'NONE', *, *, #37532, .F. ) ;
#40037=CARTESIAN_POINT ( 'NONE',  ( -29.62287095715005592, -23.40871900810292772, -1.443836166241315055 ) ) ;
#40038=CARTESIAN_POINT ( 'NONE',  ( -39.49170631829002787, -25.27985531019455578, 5.433214399821440388 ) ) ;
#40040=CARTESIAN_POINT ( 'NONE',  ( -40.47824818423304549, -24.73531770709094957, 8.716586749053510275 ) ) ;
#40042=CARTESIAN_POINT ( 'NONE',  ( 18.81927703376926786, -7.057843677351100631, 11.49999999999998934 ) ) ;
#40044=EDGE_CURVE ( 'NONE', #65926, #30754, #52614, .T. ) ;
#40045=VERTEX_POINT ( 'NONE', #91663 ) ;
#40046=CARTESIAN_POINT ( 'NONE',  ( -66.65280601721215703, -23.48786465467241058, 11.44779295918254824 ) ) ;
#40047=VECTOR ( 'NONE', #89268, 1000.000000000000114 ) ;
#40049=CARTESIAN_POINT ( 'NONE',  ( 7.334040449947802465, -21.76207178258647090, 11.49999999999999645 ) ) ;
#40050=B_SPLINE_CURVE_WITH_KNOTS ( 'NONE', 3,
 ( #11177, #49261, #26403, #80188 ),
 .UNSPECIFIED., .F., .F.,
 ( 4, 4 ),
 ( 0.3807718998933248833, 0.3897783311654404725 ),
 .UNSPECIFIED. ) ;
#40051=CARTESIAN_POINT ( 'NONE',  ( -4.086358941109507370, -22.34742993483353146, 11.49999999999998934 ) ) ;
#40052=ORIENTED_EDGE ( 'NONE', *, *, #8924, .F. ) ;
#40053=CARTESIAN_POINT ( 'NONE',  ( -109.6228709571500133, -24.51283580621365132, 0.6167428607019883602 ) ) ;
#40055=CARTESIAN_POINT ( 'NONE',  ( -98.52287095715000476, -24.51283580621364067, 0.6167428607019795894 ) ) ;
#40056=CARTESIAN_POINT ( 'NONE',  ( -40.39538329754159918, -25.19528640796965036, 3.295757161197724550 ) ) ;
#40058=ADVANCED_FACE ( 'NONE', ( #13535 ), #66365, .T. ) ;
#40059=CARTESIAN_POINT ( 'NONE',  ( -61.59189125704997281, -25.08279362854488781, 7.371166896404004909 ) ) ;
#40060=B_SPLINE_CURVE_WITH_KNOTS ( 'NONE', 3,
 ( #22273, #54261, #13666, #77065, #85190, #100392 ),
 .UNSPECIFIED., .F., .F.,
 ( 4, 2, 4 ),
 ( 6.384118678608373569E-06, 0.001386860460828372816, 0.002767336802978137555 ),
 .UNSPECIFIED. ) ;
#40062=CARTESIAN_POINT ( 'NONE',  ( -26.09636659181000695, -24.95932275238217102, 4.940287574183225061 ) ) ;
#40063=CARTESIAN_POINT ( 'NONE',  ( -61.52287095715006870, -23.94994826722564696, -0.6494450866342758033 ) ) ;
#40065=ORIENTED_EDGE ( 'NONE', *, *, #1923, .F. ) ;
#40066=CARTESIAN_POINT ( 'NONE',  ( 18.82465703714932204, -7.861812626244089053, -1.500000000000002220 ) ) ;
#40069=CARTESIAN_POINT ( 'NONE',  ( -16.88208375265294237, -15.58181570610299715, 11.49999999999998934 ) ) ;
#40074=CARTESIAN_POINT ( 'NONE',  ( -118.5228709571500758, -24.65952944569305316, 1.056160979905705899 ) ) ;
#40076=CARTESIAN_POINT ( 'NONE',  ( 20.93798385506118365, 3.901641247904229282, 11.49999999999999645 ) ) ;
#40077=VERTEX_POINT ( 'NONE', #37887 ) ;
#40078=VERTEX_POINT ( 'NONE', #6935 ) ;
#40079=CARTESIAN_POINT ( 'NONE',  ( -21.14947813473477822, 6.846651710974520633, 11.49999999999998934 ) ) ;
#40080=CARTESIAN_POINT ( 'NONE',  ( 18.87225196054570020, 8.368929400942139551, -1.500000000000002220 ) ) ;
#40081=VECTOR ( 'NONE', #92110, 1000.000000000000114 ) ;
#40084=CARTESIAN_POINT ( 'NONE',  ( -70.79417929288042899, -25.11539253604531297, 2.804427796191110378 ) ) ;
#40086=CARTESIAN_POINT ( 'NONE',  ( -127.5228709571500616, -24.64898659630368627, 1.056161002820834804 ) ) ;
#40088=CARTESIAN_POINT ( 'NONE',  ( -58.56687466182343371, -23.48786465467241413, 11.44779295918254647 ) ) ;
#40089=DIRECTION ( 'NONE',  ( 0.000000000000000000, 0.9999999999976377785, 2.173523156925979975E-06 ) ) ;
#40090=CARTESIAN_POINT ( 'NONE',  ( 2.550444227103870531, -20.70361394434535285, -1.500000000000002220 ) ) ;
#40091=CARTESIAN_POINT ( 'NONE',  ( -9.754611696910345131, 19.53525426502628548, 11.49999999999999645 ) ) ;
#40093=CARTESIAN_POINT ( 'NONE',  ( -27.47736343186643637, -24.77993795937362975, 7.597050500966643583 ) ) ;
#40095=CARTESIAN_POINT ( 'NONE',  ( 16.76845895467136671, -15.01613412638008782, 11.49999999999998934 ) ) ;
#40096=CARTESIAN_POINT ( 'NONE',  ( -118.6258445754143338, -24.15620529776628800, 10.23563542870659582 ) ) ;
#40100=ORIENTED_EDGE ( 'NONE', *, *, #86072, .T. ) ;
#40101=ORIENTED_EDGE ( 'NONE', *, *, #9948, .F. ) ;
#40103=EDGE_CURVE ( 'NONE', #99816, #30369, #71443, .T. ) ;
#40104=ORIENTED_EDGE ( 'NONE', *, *, #15983, .F. ) ;
#40105=CARTESIAN_POINT ( 'NONE',  ( -15.65470850568805083, 14.63654280257262386, -1.500000000000002220 ) ) ;
#40106=CARTESIAN_POINT ( 'NONE',  ( 19.44376294880228428, 11.01865886811674677, 11.49999999999999645 ) ) ;
#40108=VERTEX_POINT ( 'NONE', #23646 ) ;
#40110=CARTESIAN_POINT ( 'NONE',  ( 17.02745815656931683, -12.38318283856952107, 11.49999999999998934 ) ) ;
#40111=CARTESIAN_POINT ( 'NONE',  ( -30.58285055587994705, -25.15098267793663922, 7.291421475381018702 ) ) ;
#40112=CARTESIAN_POINT ( 'NONE',  ( -19.59816365915598979, -3.832847594873297403, -1.500000000000002220 ) ) ;
#40113=CARTESIAN_POINT ( 'NONE',  ( -117.6228709571500559, -23.48783264082479505, -1.443836473390058384 ) ) ;
#40115=CARTESIAN_POINT ( 'NONE',  ( 8.687672273659204691, 20.25853876245846408, -1.500000000000002220 ) ) ;
#40116=CARTESIAN_POINT ( 'NONE',  ( -83.52287095715006160, -23.47593901973090524, -1.443836447538996648 ) ) ;
#40118=DIRECTION ( 'NONE',  ( -1.000000000000000000, -3.773278334444167608E-23, -8.201307833595939069E-29 ) ) ;
#40119=CARTESIAN_POINT ( 'NONE',  ( -126.6228709571500843, -23.47596703998600631, 11.44779298504227860 ) ) ;
#40120=CARTESIAN_POINT ( 'NONE',  ( 15.14581745102402088, -14.33592658440916523, 11.49999999999999645 ) ) ;
#40123=CARTESIAN_POINT ( 'NONE',  ( -32.07722060962684196, -24.87479601683932984, 8.247789944617052171 ) ) ;
#40126=CARTESIAN_POINT ( 'NONE',  ( -16.81368161134402683, 13.12552177539105358, 11.49999999999998934 ) ) ;
#40127=LINE ( 'NONE', #48247, #93590 ) ;
#40132=CARTESIAN_POINT ( 'NONE',  ( -22.39070119279581306, -2.479732019442284496, -1.500000000000002220 ) ) ;
#40133=B_SPLINE_CURVE_WITH_KNOTS ( 'NONE', 3,
 ( #85896, #15876, #15373, #85387 ),
 .UNSPECIFIED., .F., .F.,
 ( 4, 4 ),
 ( 0.2989766979437447625, 0.2999774449845101221 ),
 .UNSPECIFIED. ) ;
#40134=B_SPLINE_SURFACE_WITH_KNOTS ( 'NONE', 3, 3, ( 
 ( #33192, #25580, #56554, #72271 ),
 ( #29069, #4748, #59040, #20951 ),
 ( #44810, #36197, #13835, #67656 ),
 ( #75243, #97585, #12346, #5239 ),
 ( #35202, #42822, #27590, #13336 ),
 ( #83352, #28577, #58541, #90476 ),
 ( #67161, #98574, #90971, #59537 ),
 ( #43317, #66173, #60042, #74742 ),
 ( #73753, #21440, #11853, #52420 ),
 ( #98069, #81369, #75730, #97092 ) ),
 .UNSPECIFIED., .F., .F., .F.,
 ( 4, 3, 3, 4 ),
 ( 4, 4 ),
 ( 0.7022005934544807149, 0.7765311282028795059, 0.8508616629512784080, 0.9995227324480762121 ),
 ( 0.5995663561115596174, 0.6009364140660176101 ),
 .UNSPECIFIED. ) ;
#40135=CARTESIAN_POINT ( 'NONE',  ( -89.06226385320381667, -25.23397913219354294, 6.409327625488849378 ) ) ;
#40136=ORIENTED_EDGE ( 'NONE', *, *, #9303, .F. ) ;
#40138=CARTESIAN_POINT ( 'NONE',  ( -31.51235681150392409, -23.73791477778911130, 11.05961554403171299 ) ) ;
#40139=CARTESIAN_POINT ( 'NONE',  ( -19.15055961920884542, -4.482958728538418924, 11.49999999999999645 ) ) ;
#40141=DIRECTION ( 'NONE',  ( 3.773278334444166432E-23, -1.000000000000000000, 0.000000000000000000 ) ) ;
#40143=CARTESIAN_POINT ( 'NONE',  ( -99.50802952236794852, -24.65952944569304961, 1.056160979905703901 ) ) ;
#40144=DIRECTION ( 'NONE',  ( -3.773278334453079618E-23, 0.9999999999976377785, 2.173523156925979975E-06 ) ) ;
#40145=CARTESIAN_POINT ( 'NONE',  ( -124.5915517817484073, -23.48786465467241769, 11.44779295918253581 ) ) ;
#40148=CARTESIAN_POINT ( 'NONE',  ( -3.970774856468506364, -19.35638658347046714, 11.49999999999998934 ) ) ;
#40150=CARTESIAN_POINT ( 'NONE',  ( 17.48260522047220888, -10.12088315688240314, 11.49999999999999645 ) ) ;
#40154=CARTESIAN_POINT ( 'NONE',  ( -48.62287095715004881, -23.72773821059535493, 11.05748984161097503 ) ) ;
#40156=CARTESIAN_POINT ( 'NONE',  ( -88.88918693012686845, -25.23397913219354649, 6.409327625488847602 ) ) ;
#40159=FACE_OUTER_BOUND ( 'NONE', #17485, .T. ) ;
#40160=DIRECTION ( 'NONE',  ( -3.773278334444167608E-23, 1.000000000000000000, 0.000000000000000000 ) ) ;
#40161=CARTESIAN_POINT ( 'NONE',  ( -16.84340083857899018, -10.81494551495373457, 11.49999999999998934 ) ) ;
#40163=CARTESIAN_POINT ( 'NONE',  ( -99.13021050592293193, -25.10935259592492841, 3.853445119336080804 ) ) ;
#40164=PLANE ( 'NONE',  #69483 ) ;
#40165=ORIENTED_EDGE ( 'NONE', *, *, #53692, .F. ) ;
#40166=B_SPLINE_CURVE_WITH_KNOTS ( 'NONE', 3,
 ( #95532, #20386, #3695, #11296 ),
 .UNSPECIFIED., .F., .F.,
 ( 4, 4 ),
 ( 0.2106504203089220317, 0.2196568515810378708 ),
 .UNSPECIFIED. ) ;
#40167=CARTESIAN_POINT ( 'NONE',  ( -79.60527230392054321, -23.48786465467241058, 11.44779295918254824 ) ) ;
#40168=DIRECTION ( 'NONE',  ( 0.000000000000000000, -0.9999999999976377785, -2.173523156925979975E-06 ) ) ;
#40170=CARTESIAN_POINT ( 'NONE',  ( -35.57119359481463050, -25.00158670708910336, 2.256160236439224143 ) ) ;
#40172=B_SPLINE_CURVE_WITH_KNOTS ( 'NONE', 3,
 ( #17686, #95805, #65888, #58259 ),
 .UNSPECIFIED., .F., .F.,
 ( 4, 4 ),
 ( 0.000000000000000000, 9.999999999998897304E-05 ),
 .UNSPECIFIED. ) ;
#40173=EDGE_CURVE ( 'NONE', #5690, #22913, #56894, .T. ) ;
#40174=CARTESIAN_POINT ( 'NONE',  ( -38.58953762381672448, -23.48783264082477373, -1.443836473390072594 ) ) ;
#40175=CARTESIAN_POINT ( 'NONE',  ( -83.62924783544907825, -24.34968618360933235, 0.1864209137778810865 ) ) ;
#40176=CARTESIAN_POINT ( 'NONE',  ( -63.62287095715007723, -24.51387760970723662, 9.387446482453425389 ) ) ;
#40177=CARTESIAN_POINT ( 'NONE',  ( -49.50841769935764347, -25.26288593538659910, 3.984447754961206734 ) ) ;
#40178=ORIENTED_EDGE ( 'NONE', *, *, #61732, .T. ) ;
#40179=CARTESIAN_POINT ( 'NONE',  ( -14.66855384320708033, -14.05595220846724835, -1.500000000000002220 ) ) ;
#40180=ADVANCED_FACE ( 'NONE', ( #53629 ), #93155, .F. ) ;
#40181=PLANE ( 'NONE',  #58265 ) ;
#40182=CARTESIAN_POINT ( 'NONE',  ( -34.50430589304357909, -23.96119346886880663, -0.6495511937831991434 ) ) ;
#40184=DIRECTION ( 'NONE',  ( 0.000000000000000000, 0.9999999999976377785, 2.173523156925979975E-06 ) ) ;
#40185=EDGE_LOOP ( 'NONE', ( #25462, #1038, #64743, #40222 ) ) ;
#40187=CARTESIAN_POINT ( 'NONE',  ( 17.50376878386636292, -9.983289808088789741, -1.500000000000002220 ) ) ;
#40188=CARTESIAN_POINT ( 'NONE',  ( -19.14942259116913092, -8.910193081567555851, 11.49999999999999645 ) ) ;
#40189=CARTESIAN_POINT ( 'NONE',  ( 5.777647480883832287, 21.37485705712154171, 11.49999999999998934 ) ) ;
#40190=CARTESIAN_POINT ( 'NONE',  ( -14.32454646668868747, 14.77526322620295929, -1.500000000000002220 ) ) ;
#40192=ORIENTED_EDGE ( 'NONE', *, *, #10508, .T. ) ;
#40196=CARTESIAN_POINT ( 'NONE',  ( -61.62287095715004881, -24.66019654487199020, 8.947790411086131712 ) ) ;
#40198=EDGE_LOOP ( 'NONE', ( #886, #82126, #38727, #85710 ) ) ;
#40200=CARTESIAN_POINT ( 'NONE',  ( -110.7960670365997373, -25.13317731662320398, 2.903215637379843894 ) ) ;
#40201=CARTESIAN_POINT ( 'NONE',  ( -127.6228709571500275, -23.48786465467242124, 11.44779295918253403 ) ) ;
#40203=CARTESIAN_POINT ( 'NONE',  ( -20.39401028033356766, -3.670942005906183692, -1.500000000000002220 ) ) ;
#40204=EDGE_CURVE ( 'NONE', #67116, #3935, #86559, .T. ) ;
#40205=CARTESIAN_POINT ( 'NONE',  ( 21.66353188042378974, 1.267531592894010739, 11.49999999999999645 ) ) ;
#40206=ORIENTED_EDGE ( 'NONE', *, *, #2614, .T. ) ;
#40208=CARTESIAN_POINT ( 'NONE',  ( -110.5115395816853692, -25.11172157007268524, 2.839984004833783438 ) ) ;
#40209=CARTESIAN_POINT ( 'NONE',  ( 8.126467401150291536, 20.86698325809501497, 11.49999999999998934 ) ) ;
#40210=VECTOR ( 'NONE', #21646, 1000.000000000000114 ) ;
#40211=FACE_OUTER_BOUND ( 'NONE', #14997, .T. ) ;
#40212=CARTESIAN_POINT ( 'NONE',  ( -101.5228709571500616, -24.50321055353803956, 9.387540953477515160 ) ) ;
#40213=EDGE_CURVE ( 'NONE', #76257, #96355, #87237, .T. ) ;
#40214=ORIENTED_EDGE ( 'NONE', *, *, #23354, .F. ) ;
#40216=CARTESIAN_POINT ( 'NONE',  ( -52.52287095715006870, -24.64965694238574656, 8.947790433994203596 ) ) ;
#40217=ORIENTED_EDGE ( 'NONE', *, *, #83658, .F. ) ;
#40219=EDGE_CURVE ( 'NONE', #86483, #59266, #20553, .T. ) ;
#40220=CARTESIAN_POINT ( 'NONE',  ( -87.52287095715006160, -23.48786465467241058, 11.44779295918254292 ) ) ;
#40222=ORIENTED_EDGE ( 'NONE', *, *, #80167, .F. ) ;
#40223=EDGE_CURVE ( 'NONE', #47759, #50913, #53280, .T. ) ;
#40224=CARTESIAN_POINT ( 'NONE',  ( -107.9228709571500673, -23.47593901973090169, -1.443836447538996648 ) ) ;
#40225=CARTESIAN_POINT ( 'NONE',  ( -7.948041996521916452, 19.69052605537007850, -1.500000000000002220 ) ) ;
#40227=CARTESIAN_POINT ( 'NONE',  ( -107.5228709571500758, -23.47596703998600631, 11.44779298504228038 ) ) ;
#40228=CARTESIAN_POINT ( 'NONE',  ( 19.23208339725441007, -10.27600428404867827, 11.49999999999998934 ) ) ;
#40229=CARTESIAN_POINT ( 'NONE',  ( -103.6308638581749051, -23.96169478059713498, 10.65365249895717881 ) ) ;
#40230=AXIS2_PLACEMENT_3D ( 'NONE', #38538, #15200, #76092 ) ;
#40231=PLANE ( 'NONE',  #85844 ) ;
#40232=CARTESIAN_POINT ( 'NONE',  ( -116.6228709571500701, -23.48783264082478794, -1.443836473390058606 ) ) ;
#40233=CARTESIAN_POINT ( 'NONE',  ( 19.81658424304261246, 9.080307684375437560, -1.500000000000002220 ) ) ;
#40237=CARTESIAN_POINT ( 'NONE',  ( -48.95684766248727726, -25.12782611306136005, 6.634937016854919101 ) ) ;
#40238=ORIENTED_EDGE ( 'NONE', *, *, #99246, .T. ) ;
#40239=ORIENTED_EDGE ( 'NONE', *, *, #1446, .T. ) ;
#40240=VECTOR ( 'NONE', #5345, 1000.000000000000114 ) ;
#40242=FACE_OUTER_BOUND ( 'NONE', #48708, .T. ) ;
#40243=CARTESIAN_POINT ( 'NONE',  ( -82.63662045704941761, -23.96119346886881019, -0.6495511937831922600 ) ) ;
#40244=CARTESIAN_POINT ( 'NONE',  ( -14.73150212448299357, 15.28860238833873808, -1.500000000000002220 ) ) ;
#40245=CARTESIAN_POINT ( 'NONE',  ( -94.62287095715005592, -23.48783264082478794, -1.443836473390063491 ) ) ;
#40246=CARTESIAN_POINT ( 'NONE',  ( -130.5728709571500588, -24.43626637953623515, 0.1835287498755961699 ) ) ;
#40248=B_SPLINE_CURVE_WITH_KNOTS ( 'NONE', 3,
 ( #47966, #85511, #78890, #70803, #47464, #40348 ),
 .UNSPECIFIED., .F., .F.,
 ( 4, 2, 4 ),
 ( 0.000000000000000000, 0.001380901958385396351, 0.002761803916770792702 ),
 .UNSPECIFIED. ) ;
#40249=CARTESIAN_POINT ( 'NONE',  ( -99.52287095715006160, -24.64898659630529565, 1.056161002820829697 ) ) ;
#40250=EDGE_CURVE ( 'NONE', #73517, #99512, #79441, .T. ) ;
#40251=CARTESIAN_POINT ( 'NONE',  ( -1.608633542659107629, -19.34071428503001755, -1.500000000000002220 ) ) ;
#40252=CARTESIAN_POINT ( 'NONE',  ( -80.52287095715006160, -23.48786465467241769, 11.44779295918254469 ) ) ;
#40253=VERTEX_POINT ( 'NONE', #27168 ) ;
#40254=CARTESIAN_POINT ( 'NONE',  ( -10.96721834449554933, 16.09610527815933168, 11.49999999999999645 ) ) ;
#40256=EDGE_CURVE ( 'NONE', #77563, #51201, #39980, .T. ) ;
#40257=LINE ( 'NONE', #47370, #85211 ) ;
#40259=CARTESIAN_POINT ( 'NONE',  ( -93.62287095715004170, -23.72747288104442376, -1.053458166803661999 ) ) ;
#40260=EDGE_CURVE ( 'NONE', #99388, #64065, #4938, .T. ) ;
#40261=CARTESIAN_POINT ( 'NONE',  ( -89.51816582126249955, -23.73766607897671221, -1.055555164236434473 ) ) ;
#40263=FACE_OUTER_BOUND ( 'NONE', #34629, .T. ) ;
#40264=CARTESIAN_POINT ( 'NONE',  ( -19.61143073682725202, -1.510137823221562092, 11.49999999999998934 ) ) ;
#40265=B_SPLINE_SURFACE_WITH_KNOTS ( 'NONE', 3, 3, ( 
 ( #42760, #20887, #81307, #42276 ),
 ( #75178, #88927, #51863, #82794 ),
 ( #82299, #5673, #19398, #13275 ),
 ( #36623, #12778, #89917, #11790 ),
 ( #67591, #73206, #74683, #66112 ),
 ( #67101, #34641, #98008, #89420 ),
 ( #73695, #98508, #29006, #59978 ),
 ( #90912, #35639, #27528, #21379 ),
 ( #3694, #4189, #58484, #80811 ),
 ( #20385, #19893, #50866, #81804 ) ),
 .UNSPECIFIED., .F., .F., .F.,
 ( 4, 3, 3, 4 ),
 ( 4, 4 ),
 ( 0.0004766839783813265198, 0.1491231665100168635, 0.2234464077758346323, 0.2977696490416523734 ),
 ( 0.4495482928597397398, 0.4508289012804921891 ),
 .UNSPECIFIED. ) ;
#40267=CARTESIAN_POINT ( 'NONE',  ( -8.750087785235610482, 19.73178376063210138, 11.49999999999998934 ) ) ;
#40268=CARTESIAN_POINT ( 'NONE',  ( -65.52287095715006160, -25.00182538069144655, 7.747789668545101982 ) ) ;
#40269=CARTESIAN_POINT ( 'NONE',  ( -46.55620429048340014, -23.47593901973091235, -1.443836447539009749 ) ) ;
#40271=CARTESIAN_POINT ( 'NONE',  ( -93.54470913934721921, -24.65952944569305316, 1.056160979905699904 ) ) ;
#40272=CARTESIAN_POINT ( 'NONE',  ( -105.6228709571500559, -23.84081130438201157, 10.88220057463249013 ) ) ;
#40273=CARTESIAN_POINT ( 'NONE',  ( -97.59120377316065742, -24.15620529776629155, 10.23563542870660115 ) ) ;
#40274=CARTESIAN_POINT ( 'NONE',  ( -100.6365410905178379, -25.04435010277327933, 7.557279746904548290 ) ) ;
#40276=DIRECTION ( 'NONE',  ( 0.000000000000000000, -0.9999999999976377785, -2.173523156925979128E-06 ) ) ;
#40277=CARTESIAN_POINT ( 'NONE',  ( -114.5192661640313503, -23.96169478059714564, 10.65365249895717170 ) ) ;
#40278=CARTESIAN_POINT ( 'NONE',  ( -5.841000908416043913, -19.03464889989004050, -1.500000000000002220 ) ) ;
#40279=EDGE_CURVE ( 'NONE', #50558, #36016, #96182, .T. ) ;
#40280=CARTESIAN_POINT ( 'NONE',  ( -75.61136356471840259, -23.48786465467241058, 11.44779295918254824 ) ) ;
#40281=CARTESIAN_POINT ( 'NONE',  ( 19.41305359857673096, 4.112862643401165919, -1.500000000000002220 ) ) ;
#40283=AXIS2_PLACEMENT_3D ( 'NONE', #88589, #40908, #25174 ) ;
#40286=CARTESIAN_POINT ( 'NONE',  ( -50.40445135320378967, -25.13313949306887451, 7.101635536975466678 ) ) ;
#40288=CARTESIAN_POINT ( 'NONE',  ( -2.856624844580134770, 20.53689577262001364, 11.49999999999999645 ) ) ;
#40290=ADVANCED_FACE ( 'NONE', ( #49515 ), #41907, .F. ) ;
#40291=CARTESIAN_POINT ( 'NONE',  ( -62.62287095715004881, -29.50248528299804818, 1.056150453629034924 ) ) ;
#40292=CARTESIAN_POINT ( 'NONE',  ( -13.85039312988123150, 18.09399583546626289, 11.49999999999999645 ) ) ;
#40294=CARTESIAN_POINT ( 'NONE',  ( -57.62287095715007013, -23.96127896941631619, -0.6493128931037834839 ) ) ;
#40296=CARTESIAN_POINT ( 'NONE',  ( -38.52287095715006870, -24.65952944569303895, 1.056160979905691910 ) ) ;
#40297=VERTEX_POINT ( 'NONE', #57134 ) ;
#40298=AXIS2_PLACEMENT_3D ( 'NONE', #21557, #45424, #59150 ) ;
#40299=CARTESIAN_POINT ( 'NONE',  ( 4.066846734877469949, -19.79409818376439389, -1.500000000000002220 ) ) ;
#40302=CARTESIAN_POINT ( 'NONE',  ( -114.5228709571500190, -24.66019654487200441, 8.947790411086110396 ) ) ;
#40303=EDGE_CURVE ( 'NONE', #51581, #99250, #9783, .T. ) ;
#40304=VERTEX_POINT ( 'NONE', #3838 ) ;
#40305=CARTESIAN_POINT ( 'NONE',  ( -10.30982817980528132, -21.98926139291980064, 11.50200000000000422 ) ) ;
#40306=CARTESIAN_POINT ( 'NONE',  ( -10.62949710387652758, 20.32685691788189075, -1.500000000000002220 ) ) ;
#40308=CARTESIAN_POINT ( 'NONE',  ( 18.82558416981596139, 6.732768832687442639, -1.500000000000002220 ) ) ;
#40310=CARTESIAN_POINT ( 'NONE',  ( 17.09260067683297635, -12.12037977771017871, 11.49999999999999645 ) ) ;
#40311=CARTESIAN_POINT ( 'NONE',  ( -59.90086283640256681, -25.29841105421058955, 4.072422571224184829 ) ) ;
#40313=CARTESIAN_POINT ( 'NONE',  ( -3.902479932019291553, -21.71820464621639246, -1.500000000000002220 ) ) ;
#40317=CARTESIAN_POINT ( 'NONE',  ( -49.63711845704647629, -25.18440172823959955, 3.620155769584360694 ) ) ;
#40320=CARTESIAN_POINT ( 'NONE',  ( -103.6228709571500559, -29.50250786944525672, 11.44777988621623166 ) ) ;
#40321=B_SPLINE_CURVE_WITH_KNOTS ( 'NONE', 3,
 ( #16415, #83942, #77804, #92547 ),
 .UNSPECIFIED., .F., .F.,
 ( 4, 4 ),
 ( 0.7410291507779422915, 0.7500355820500579362 ),
 .UNSPECIFIED. ) ;
#40324=CARTESIAN_POINT ( 'NONE',  ( -99.62287095715005592, -23.48783264082478794, -1.443836473390061936 ) ) ;
#40325=CARTESIAN_POINT ( 'NONE',  ( -85.22287095715010707, -23.47593901973090524, -1.443836447538997314 ) ) ;
#40326=CARTESIAN_POINT ( 'NONE',  ( -36.63503066435342248, -24.34968618360933590, 0.1864209137778783110 ) ) ;
#40327=CARTESIAN_POINT ( 'NONE',  ( -14.38416181709762043, 14.64695106392160895, -1.500000000000002220 ) ) ;
#40331=CARTESIAN_POINT ( 'NONE',  ( -41.52287095715006870, -23.72773821059536203, 11.05748984161097326 ) ) ;
#40332=CARTESIAN_POINT ( 'NONE',  ( -21.62769966018443313, 5.350386031573528989, 11.49999999999998934 ) ) ;
#40336=ORIENTED_EDGE ( 'NONE', *, *, #31661, .T. ) ;
#40337=CARTESIAN_POINT ( 'NONE',  ( -96.62287095715009855, -23.96127896941631619, -0.6493128931037810414 ) ) ;
#40339=CARTESIAN_POINT ( 'NONE',  ( -18.77111393065419875, 9.022841878967760465, -1.500000000000002220 ) ) ;
#40340=VERTEX_POINT ( 'NONE', #26667 ) ;
#40341=B_SPLINE_CURVE_WITH_KNOTS ( 'NONE', 3,
 ( #10785, #57975, #66098, #50352, #58963, #97015 ),
 .UNSPECIFIED., .F., .F.,
 ( 4, 2, 4 ),
 ( 1.570755371634131319E-05, 0.001396183895866089054, 0.002776660238015836880 ),
 .UNSPECIFIED. ) ;
#40343=VERTEX_POINT ( 'NONE', #71847 ) ;
#40345=CARTESIAN_POINT ( 'NONE',  ( -69.11592688286732766, -25.25935203297461484, 6.884840302703743475 ) ) ;
#40346=CARTESIAN_POINT ( 'NONE',  ( -3.838044578953509145, 20.63102806057878880, -1.500000000000002220 ) ) ;
#40347=VERTEX_POINT ( 'NONE', #50017 ) ;
#40348=CARTESIAN_POINT ( 'NONE',  ( -118.5228709571500758, -23.47596703998600631, 11.44779298504227860 ) ) ;
#40349=AXIS2_PLACEMENT_3D ( 'NONE', #37809, #61167, #99681 ) ;
#40353=CARTESIAN_POINT ( 'NONE',  ( -101.7635726060833434, -25.03152285269965915, 6.809096594898544907 ) ) ;
#40354=CARTESIAN_POINT ( 'NONE',  ( -59.58754539228643665, -24.34968618360933235, 0.1864209137778795600 ) ) ;
#40355=CARTESIAN_POINT ( 'NONE',  ( -108.9857487368351627, -25.30480944508042640, 4.484590831594999827 ) ) ;
#40356=DIRECTION ( 'NONE',  ( -3.773278334453079030E-23, 0.9999999999976377785, 2.173523156925979128E-06 ) ) ;
#40357=CARTESIAN_POINT ( 'NONE',  ( -22.22723998432330106, 0.1330083165726352878, 11.49999999999999645 ) ) ;
#40358=EDGE_LOOP ( 'NONE', ( #66506, #32979, #35070, #64486 ) ) ;
#40360=LINE ( 'NONE', #26132, #60246 ) ;
#40361=ORIENTED_EDGE ( 'NONE', *, *, #67711, .T. ) ;
#40362=CARTESIAN_POINT ( 'NONE',  ( -2.225104987405961854, -22.55768739424384606, 11.49999999999998934 ) ) ;
#40365=ORIENTED_EDGE ( 'NONE', *, *, #99608, .T. ) ;
#40367=VECTOR ( 'NONE', #5211, 1000.000000000000114 ) ;
#40369=EDGE_CURVE ( 'NONE', #52307, #21700, #78, .T. ) ;
#40370=CARTESIAN_POINT ( 'NONE',  ( 9.931738293602487389, -17.53800358597336384, 11.49999999999998934 ) ) ;
#40371=CARTESIAN_POINT ( 'NONE',  ( -32.62287095715007013, -24.51283580621364777, 0.6167428607019671549 ) ) ;
#40373=CARTESIAN_POINT ( 'NONE',  ( -58.55620429048338593, -23.48783264082478439, -1.443836473390070596 ) ) ;
#40374=CARTESIAN_POINT ( 'NONE',  ( 22.37589550080693712, 1.095942408959037273, -1.500000000000002220 ) ) ;
#40375=ORIENTED_EDGE ( 'NONE', *, *, #60326, .T. ) ;
#40376=VERTEX_POINT ( 'NONE', #58618 ) ;
#40378=CARTESIAN_POINT ( 'NONE',  ( -69.52287095715006160, -24.64965694238407323, 8.947790433994200043 ) ) ;
#40379=DIRECTION ( 'NONE',  ( 3.773278334444166432E-23, -1.000000000000000000, 0.000000000000000000 ) ) ;
#40380=EDGE_CURVE ( 'NONE', #57758, #13348, #69084, .T. ) ;
#40381=ADVANCED_FACE ( 'NONE', ( #43397 ), #36279, .F. ) ;
#40382=LINE ( 'NONE', #3829, #35200 ) ;
#40384=CARTESIAN_POINT ( 'NONE',  ( -130.5728709571500588, -23.47593901973090524, -1.443836447538995760 ) ) ;
#40385=CARTESIAN_POINT ( 'NONE',  ( -19.37596289572233488, 2.755671585415585767, -1.500000000000002220 ) ) ;
#40387=VERTEX_POINT ( 'NONE', #89561 ) ;
#40389=CARTESIAN_POINT ( 'NONE',  ( 20.90071823198991297, 5.034746273075951351, -1.500000000000002220 ) ) ;
#40390=CARTESIAN_POINT ( 'NONE',  ( -36.52287095715006870, -23.48783264082477018, -1.443836473390097019 ) ) ;
#40393=DIRECTION ( 'NONE',  ( 0.000000000000000000, -2.173523156925979552E-06, 0.9999999999976378895 ) ) ;
#40394=CARTESIAN_POINT ( 'NONE',  ( -22.88579126497628025, -1.409509213828211927, -1.500000000000002220 ) ) ;
#40398=CARTESIAN_POINT ( 'NONE',  ( -42.52287095715005449, -24.34917612407031839, 0.1852690917477345378 ) ) ;
#40399=CARTESIAN_POINT ( 'NONE',  ( -18.86779840422491716, -6.689013621249945807, 11.49999999999999645 ) ) ;
#40400=CARTESIAN_POINT ( 'NONE',  ( -78.94637683104262749, -25.31594602001839078, 5.821637659726635938 ) ) ;
#40401=DIRECTION ( 'NONE',  ( -3.773278334453079618E-23, 0.9999999999976377785, 2.173523156925979975E-06 ) ) ;
#40403=CARTESIAN_POINT ( 'NONE',  ( -39.62287095715005592, -23.47596703998600276, 11.44779298504227505 ) ) ;
#40406=CARTESIAN_POINT ( 'NONE',  ( 1.937016913031804455, -21.67664703184077268, 11.49999999999998934 ) ) ;
#40408=CARTESIAN_POINT ( 'NONE',  ( 16.09843989366402539, -11.26760994518913428, -1.500000000000002220 ) ) ;
#40409=DIRECTION ( 'NONE',  ( -0.000000000000000000, 2.173523156925979552E-06, -0.9999999999976378895 ) ) ;
#40410=EDGE_CURVE ( 'NONE', #623, #27902, #20531, .T. ) ;
#40411=PLANE ( 'NONE',  #45094 ) ;
#40413=CARTESIAN_POINT ( 'NONE',  ( -91.63415563865659408, -23.96169478059713498, 10.65365249895717881 ) ) ;
#40415=CARTESIAN_POINT ( 'NONE',  ( -12.99546161633903552, -15.93940442571882876, 11.49999999999999645 ) ) ;
#40417=EDGE_CURVE ( 'NONE', #48044, #98355, #19541, .T. ) ;
#40418=CARTESIAN_POINT ( 'NONE',  ( -120.6238000549733727, -24.92564183028979485, 1.928384488918253092 ) ) ;
#40419=CARTESIAN_POINT ( 'NONE',  ( 19.13181028273733375, 12.02906595412573232, 11.49999999999999645 ) ) ;
#40421=CARTESIAN_POINT ( 'NONE',  ( -100.6258216950799778, -25.26387453630955449, 4.735305889788031131 ) ) ;
#40422=PLANE ( 'NONE',  #31525 ) ;
#40423=CARTESIAN_POINT ( 'NONE',  ( -97.59120735429435456, -24.15543982623907837, -0.2315651400026600415 ) ) ;
#40424=CARTESIAN_POINT ( 'NONE',  ( -72.62287095715004170, -23.72773821059535848, 11.05748984161097681 ) ) ;
#40426=CARTESIAN_POINT ( 'NONE',  ( -25.68888630310901178, -24.93063242766984544, 6.447529969727213484 ) ) ;
#40427=EDGE_CURVE ( 'NONE', #42580, #86491, #30256, .T. ) ;
#40430=EDGE_CURVE ( 'NONE', #92347, #13191, #91051, .T. ) ;
#40432=CARTESIAN_POINT ( 'NONE',  ( -80.31352994281894553, -25.26749876826690056, 4.969670918755285882 ) ) ;
#40433=CARTESIAN_POINT ( 'NONE',  ( 4.459850365305920938, 22.40387240153798487, 11.49999999999998934 ) ) ;
#40434=CARTESIAN_POINT ( 'NONE',  ( -110.5228709571500616, -24.99156044556120548, 7.747789690856173195 ) ) ;
#40436=CARTESIAN_POINT ( 'NONE',  ( -72.58953762381671027, -24.66019654487198665, 8.947790411086131712 ) ) ;
#40437=CARTESIAN_POINT ( 'NONE',  ( -82.62631727302549223, -24.51419770103156281, 9.386484678747187615 ) ) ;
#40438=CARTESIAN_POINT ( 'NONE',  ( -15.54266751046811557, -16.22994250641250957, 11.49999999999999645 ) ) ;
#40440=AXIS2_PLACEMENT_3D ( 'NONE', #85846, #92943, #93443 ) ;
#40442=CARTESIAN_POINT ( 'NONE',  ( -21.18249553426131015, -5.656070447573528170, -1.500000000000002220 ) ) ;
#40444=AXIS2_PLACEMENT_3D ( 'NONE', #41757, #72701, #3197 ) ;
#40451=CARTESIAN_POINT ( 'NONE',  ( -20.44062828730913139, -1.133067592104922694, 11.49999999999998934 ) ) ;
#40452=EDGE_LOOP ( 'NONE', ( #64155, #97961, #36442, #99264 ) ) ;
#40454=ORIENTED_EDGE ( 'NONE', *, *, #30636, .T. ) ;
#40456=B_SPLINE_CURVE_WITH_KNOTS ( 'NONE', 3,
 ( #20368, #4171, #51343, #43731 ),
 .UNSPECIFIED., .F., .F.,
 ( 4, 4 ),
 ( 1.387778780781445521E-17, 9.999999999997510880E-05 ),
 .UNSPECIFIED. ) ;
#40457=CARTESIAN_POINT ( 'NONE',  ( 21.72910700495702230, 7.846448622349001312, -1.500000000000002220 ) ) ;
#40458=CARTESIAN_POINT ( 'NONE',  ( -112.5228709571500616, -24.66019654487200441, 8.947790411086108620 ) ) ;
#40459=CARTESIAN_POINT ( 'NONE',  ( -6.692510123977180925, 19.25193956699996178, -1.500000000000002220 ) ) ;
#40463=CARTESIAN_POINT ( 'NONE',  ( -116.6228709571500559, -29.50248528299804818, 1.056150453629045360 ) ) ;
#40464=CARTESIAN_POINT ( 'NONE',  ( -70.57802201159600486, -25.00158670708910691, 2.256160236439221034 ) ) ;
#40465=CARTESIAN_POINT ( 'NONE',  ( -5.607854029519995898, -20.77141283803394955, 11.49999999999999645 ) ) ;
#40466=ORIENTED_EDGE ( 'NONE', *, *, #99934, .F. ) ;
#40467=CARTESIAN_POINT ( 'NONE',  ( -75.58921274596343665, -24.52300882791530512, 0.6510814631126415897 ) ) ;
#40468=CARTESIAN_POINT ( 'NONE',  ( -48.55620429048338593, -24.64898659630528144, 1.056161002820819927 ) ) ;
#40469=VERTEX_POINT ( 'NONE', #37272 ) ;
#40470=CARTESIAN_POINT ( 'NONE',  ( 3.485566553294195291, 20.44204155273375889, 11.49999999999998934 ) ) ;
#40471=ORIENTED_EDGE ( 'NONE', *, *, #68820, .T. ) ;
#40472=CARTESIAN_POINT ( 'NONE',  ( -125.5887523808240047, -25.00158670708911046, 2.256160236439218369 ) ) ;
#40475=CARTESIAN_POINT ( 'NONE',  ( -53.52287095715004739, -24.34917612406836440, 0.1852690917426514372 ) ) ;
#40476=EDGE_LOOP ( 'NONE', ( #18672, #4509, #77188, #59034 ) ) ;
#40478=CARTESIAN_POINT ( 'NONE',  ( -40.52287095715006160, -23.85196035786899671, -0.8779234886475247857 ) ) ;
#40479=FACE_OUTER_BOUND ( 'NONE', #28985, .T. ) ;
#40480=DIRECTION ( 'NONE',  ( 3.773278334444166432E-23, -1.000000000000000000, 0.000000000000000000 ) ) ;
#40481=CARTESIAN_POINT ( 'NONE',  ( 21.39010012190943755, 5.354582491813655309, 11.49999999999999645 ) ) ;
#40482=VERTEX_POINT ( 'NONE', #28165 ) ;
#40483=CARTESIAN_POINT ( 'NONE',  ( -103.6332059738791003, -23.73766607897670156, -1.055555164236454901 ) ) ;
#40484=CARTESIAN_POINT ( 'NONE',  ( -10.21242994381667657, -20.12718729479640700, -1.500000000000002220 ) ) ;
#40485=CARTESIAN_POINT ( 'NONE',  ( 20.48634023128459347, 4.603634630958829632, -1.500000000000002220 ) ) ;
#40486=B_SPLINE_CURVE_WITH_KNOTS ( 'NONE', 3,
 ( #59105, #96647, #51483, #35265, #96159, #12404 ),
 .UNSPECIFIED., .F., .F.,
 ( 4, 2, 4 ),
 ( 0.000000000000000000, 0.001380901958385393966, 0.002761803916770787931 ),
 .UNSPECIFIED. ) ;
#40487=B_SPLINE_CURVE_WITH_KNOTS ( 'NONE', 3,
 ( #87441, #50392, #96060, #89445 ),
 .UNSPECIFIED., .F., .F.,
 ( 4, 4 ),
 ( 0.7010005673463182152, 0.7100069986184336379 ),
 .UNSPECIFIED. ) ;
#40488=CARTESIAN_POINT ( 'NONE',  ( -62.52287095715006160, -24.64898659630367561, 1.056161002820822592 ) ) ;
#40489=ORIENTED_EDGE ( 'NONE', *, *, #66521, .F. ) ;
#40494=ORIENTED_EDGE ( 'NONE', *, *, #69839, .F. ) ;
#40495=CARTESIAN_POINT ( 'NONE',  ( 8.100108036306837178, -19.54698220168213041, -1.500000000000002220 ) ) ;
#40497=EDGE_CURVE ( 'NONE', #9106, #48044, #16775, .T. ) ;
#40498=CARTESIAN_POINT ( 'NONE',  ( -51.20402663469029392, -25.26041081037891445, 7.397223726173897340 ) ) ;
#40500=CARTESIAN_POINT ( 'NONE',  ( -75.62287095715008434, -24.14321612903114556, -0.2833117244521566325 ) ) ;
#40501=CARTESIAN_POINT ( 'NONE',  ( -125.6228709571500559, -24.99132157543083821, 2.256160258750667502 ) ) ;
#40502=CARTESIAN_POINT ( 'NONE',  ( -47.62287095715004170, -23.72773821059535493, 11.05748984161097503 ) ) ;
#40503=CARTESIAN_POINT ( 'NONE',  ( 22.17158117043571863, -1.905908075979310334, -1.500000000000002220 ) ) ;
#40504=EDGE_CURVE ( 'NONE', #99512, #25851, #95499, .T. ) ;
#40505=CARTESIAN_POINT ( 'NONE',  ( -49.87826110250815503, -25.13941482721087084, 7.497148031602994145 ) ) ;
#40506=ADVANCED_FACE ( 'NONE', ( #74335 ), #5815, .T. ) ;
#40507=ORIENTED_EDGE ( 'NONE', *, *, #44976, .F. ) ;
#40509=CARTESIAN_POINT ( 'NONE',  ( -37.62900166493126619, -24.51314013834315375, 0.6176544820404124003 ) ) ;
#40511=AXIS2_PLACEMENT_3D ( 'NONE', #68690, #22484, #29117 ) ;
#40512=ADVANCED_FACE ( 'NONE', ( #67738 ), #22421, .T. ) ;
#40517=CARTESIAN_POINT ( 'NONE',  ( 18.70946937610417038, -5.484834493922766896, -1.500000000000002220 ) ) ;
#40519=CARTESIAN_POINT ( 'NONE',  ( 14.52366289275476419, -15.72616519631134580, 11.49999999999998934 ) ) ;
#40521=FACE_OUTER_BOUND ( 'NONE', #87916, .T. ) ;
#40522=CARTESIAN_POINT ( 'NONE',  ( -100.6228709571500701, -24.83620972994592790, 8.398175272781362111 ) ) ;
#40524=CARTESIAN_POINT ( 'NONE',  ( -22.07869367785253090, -5.390224856484156390, -1.500000000000002220 ) ) ;
#40525=AXIS2_PLACEMENT_3D ( 'NONE', #99380, #15147, #30877 ) ;
#40526=CARTESIAN_POINT ( 'NONE',  ( -98.59116248804129157, -24.15543982623907837, -0.2315651400026625395 ) ) ;
#40527=FACE_OUTER_BOUND ( 'NONE', #29292, .T. ) ;
#40528=CARTESIAN_POINT ( 'NONE',  ( 1.822157996128044299, -19.77364354024053839, 11.49999999999999645 ) ) ;
#40530=B_SPLINE_CURVE_WITH_KNOTS ( 'NONE', 3,
 ( #39626, #1074, #64001, #48256, #53864, #39122, #54866, #15279, #87811, #89309, #35530, #65002, #73587, #74088 ),
 .UNSPECIFIED., .F., .F.,
 ( 4, 2, 2, 2, 2, 2, 4 ),
 ( 0.000000000000000000, 0.0002088823906780594799, 0.0004177647813561189598, 0.0008355295627122259934, 0.001253294344068333135, 0.001462176734746396247, 0.001671059125424459143 ),
 .UNSPECIFIED. ) ;
#40531=CARTESIAN_POINT ( 'NONE',  ( -88.55620429048339304, -24.64898659630529210, 1.056161002820829919 ) ) ;
#40534=CARTESIAN_POINT ( 'NONE',  ( -49.31756476722683402, -25.22308043492110485, 6.418058605870250233 ) ) ;
#40536=CARTESIAN_POINT ( 'NONE',  ( -75.62287095715004170, -24.99132157543084176, 2.256160258750667502 ) ) ;
#40537=CARTESIAN_POINT ( 'NONE',  ( -17.53059066697263546, 12.75712217820542627, -1.500000000000002220 ) ) ;
#40538=CARTESIAN_POINT ( 'NONE',  ( -56.52206863758583921, -23.48786465467241058, 11.44779295918254647 ) ) ;
#40539=CARTESIAN_POINT ( 'NONE',  ( 10.22484414329051994, 16.58839404647166660, -1.500000000000002220 ) ) ;
#40540=DIRECTION ( 'NONE',  ( 1.000000000000000000, 3.773278334444167608E-23, 8.201307833595939069E-29 ) ) ;
#40543=CARTESIAN_POINT ( 'NONE',  ( -10.90597124047809530, 17.21661415904998904, 11.49999999999999645 ) ) ;
#40544=CARTESIAN_POINT ( 'NONE',  ( -110.5228709571500616, -23.48783264082477018, -1.443836473390086583 ) ) ;
#40545=CARTESIAN_POINT ( 'NONE',  ( -41.55620429048340014, -23.47593901973091235, -1.443836447539011525 ) ) ;
#40547=CARTESIAN_POINT ( 'NONE',  ( -41.46036410897617941, -25.27941668849123147, 4.063043375333840856 ) ) ;
#40549=CARTESIAN_POINT ( 'NONE',  ( -34.52287095715006160, -24.65952944569303895, 1.056160979905690134 ) ) ;
#40550=CARTESIAN_POINT ( 'NONE',  ( -49.32129151558435609, -25.25138820444266230, 5.877611043602244401 ) ) ;
#40551=CARTESIAN_POINT ( 'NONE',  ( -86.52287095715006160, -24.65952944569304606, 1.056160979905700570 ) ) ;
#40552=CARTESIAN_POINT ( 'NONE',  ( 18.22116949570664701, -8.484823103377051368, 11.49999999999998934 ) ) ;
#40554=EDGE_LOOP ( 'NONE', ( #7234, #74612, #94034, #63349 ) ) ;
#40555=CARTESIAN_POINT ( 'NONE',  ( -102.5228709571500758, -29.50248528299804818, 1.056150453629042030 ) ) ;
#40556=EDGE_CURVE ( 'NONE', #52078, #66467, #8817, .T. ) ;
#40557=CARTESIAN_POINT ( 'NONE',  ( -0.4961427919413599064, 22.93664481792237453, 11.49999999999999645 ) ) ;
#40558=CARTESIAN_POINT ( 'NONE',  ( 19.62911079104473444, -11.51699945595908758, 11.49999999999998934 ) ) ;
#40559=ORIENTED_EDGE ( 'NONE', *, *, #40410, .T. ) ;
#40560=CARTESIAN_POINT ( 'NONE',  ( -78.62287095715005592, -23.47596703998600631, 11.44779298504227860 ) ) ;
#40561=DIRECTION ( 'NONE',  ( -3.773278334453079030E-23, 0.9999999999976377785, 2.173523156925979128E-06 ) ) ;
#40562=CARTESIAN_POINT ( 'NONE',  ( -90.54438304270964011, -24.73486907724917927, 1.287355809206966573 ) ) ;
#40563=CARTESIAN_POINT ( 'NONE',  ( -30.57287095715007652, -25.15787655275395807, 6.970815268604743764 ) ) ;
#40564=AXIS2_PLACEMENT_3D ( 'NONE', #87370, #85874, #55434 ) ;
#40565=EDGE_CURVE ( 'NONE', #30069, #20120, #83938, .T. ) ;
#40566=CARTESIAN_POINT ( 'NONE',  ( -69.64549865058073408, -23.73791477778911840, 11.05961554403170766 ) ) ;
#40568=CARTESIAN_POINT ( 'NONE',  ( -122.5545149021958906, -24.34968618360934300, 0.1864209137778895797 ) ) ;
#40569=CARTESIAN_POINT ( 'NONE',  ( -81.62287095715005592, -23.47593901973091235, -1.443836447539004642 ) ) ;
#40571=CARTESIAN_POINT ( 'NONE',  ( -5.191926799570463658, 19.71030214607805675, 11.49999999999998934 ) ) ;
#40573=EDGE_LOOP ( 'NONE', ( #82117, #28997, #68433, #13964 ) ) ;
#40574=CARTESIAN_POINT ( 'NONE',  ( -15.77545706029219730, -16.76941864122914083, -1.500000000000002220 ) ) ;
#40577=CARTESIAN_POINT ( 'NONE',  ( -108.5571773441287888, -23.73791477778912196, 11.05961554403169878 ) ) ;
#40578=CARTESIAN_POINT ( 'NONE',  ( -99.52287095715006160, -24.64965694238407323, 8.947790433994194714 ) ) ;
#40580=CARTESIAN_POINT ( 'NONE',  ( -95.55787989783573266, -23.85016227208581441, -0.8807180028928280890 ) ) ;
#40582=CARTESIAN_POINT ( 'NONE',  ( -1.376967878889499897, 21.29249089469206524, 11.49999999999999645 ) ) ;
#40583=EDGE_LOOP ( 'NONE', ( #15324, #31367, #58809, #82845 ) ) ;
#40585=VERTEX_POINT ( 'NONE', #91546 ) ;
#40586=CARTESIAN_POINT ( 'NONE',  ( -19.03210976516136554, 11.49075778266564107, 11.49999999999998934 ) ) ;
#40587=CARTESIAN_POINT ( 'NONE',  ( 20.28538307770854487, 3.844468116359331944, 11.49999999999998934 ) ) ;
#40588=VECTOR ( 'NONE', #84551, 1000.000000000000227 ) ;
#40589=VERTEX_POINT ( 'NONE', #54002 ) ;
#40590=CARTESIAN_POINT ( 'NONE',  ( -41.46611000704998418, -25.28830591450888932, 4.188173661249235735 ) ) ;
#40592=AXIS2_PLACEMENT_3D ( 'NONE', #45063, #14588, #21692 ) ;
#40594=DIRECTION ( 'NONE',  ( -3.773278334453079618E-23, 0.9999999999976377785, 2.173523156925979975E-06 ) ) ;
#40595=ORIENTED_EDGE ( 'NONE', *, *, #10468, .F. ) ;
#40596=LINE ( 'NONE', #54323, #94965 ) ;
#40598=CARTESIAN_POINT ( 'NONE',  ( -18.00717387566553995, 10.56535500573724740, -1.500000000000002220 ) ) ;
#40599=CARTESIAN_POINT ( 'NONE',  ( 3.337383349182757364, -21.60657791699550856, 11.49999999999999645 ) ) ;
#40600=PLANE ( 'NONE',  #60954 ) ;
#40602=CARTESIAN_POINT ( 'NONE',  ( 9.993301969596378953, 20.15287186522775542, 11.49999999999998934 ) ) ;
#40603=CARTESIAN_POINT ( 'NONE',  ( -118.5893566070612621, -24.35071581493543746, 9.817618358456019934 ) ) ;
#40604=CARTESIAN_POINT ( 'NONE',  ( -72.52287095715007581, -23.48786465467241058, 11.44779295918254647 ) ) ;
#40606=VERTEX_POINT ( 'NONE', #68722 ) ;
#40607=ORIENTED_EDGE ( 'NONE', *, *, #63427, .T. ) ;
#40608=VERTEX_POINT ( 'NONE', #22019 ) ;
#40609=CARTESIAN_POINT ( 'NONE',  ( -100.3181550757389147, -25.12215674754353856, 7.099295233261272209 ) ) ;
#40610=ORIENTED_EDGE ( 'NONE', *, *, #43495, .F. ) ;
#40611=CARTESIAN_POINT ( 'NONE',  ( -19.04320821261859464, -9.809917703373946196, -1.500000000000002220 ) ) ;
#40612=CARTESIAN_POINT ( 'NONE',  ( 10.24050353823403192, -19.87907451059620456, 11.49999999999999645 ) ) ;
#40615=CARTESIAN_POINT ( 'NONE',  ( 3.661087877195506213, -20.73962600213626217, -1.500000000000002220 ) ) ;
#40616=CARTESIAN_POINT ( 'NONE',  ( -30.63484830301900175, -23.79244928165773842, 10.97490056816818971 ) ) ;
#40618=CARTESIAN_POINT ( 'NONE',  ( -17.52048005523606022, -9.576713672051738513, -1.500000000000002220 ) ) ;
#40620=CARTESIAN_POINT ( 'NONE',  ( -43.52287095715008292, -23.96177878511307924, 10.65340807706330573 ) ) ;
#40621=CARTESIAN_POINT ( 'NONE',  ( -10.85839155550747392, 19.17434714687634667, -1.500000000000002220 ) ) ;
#40623=CARTESIAN_POINT ( 'NONE',  ( -65.66192790180473082, -23.48786465467241058, 11.44779295918254824 ) ) ;
#40626=CARTESIAN_POINT ( 'NONE',  ( 11.47802407633690258, -17.41396394059345454, 11.49999999999999645 ) ) ;
#40629=EDGE_CURVE ( 'NONE', #73668, #66916, #55620, .T. ) ;
#40631=CARTESIAN_POINT ( 'NONE',  ( -61.52287095715006160, -24.65952944569304606, 1.056160979905695463 ) ) ;
#40632=CARTESIAN_POINT ( 'NONE',  ( -1.376967878889499897, 21.29249089469206524, 11.49999999999998934 ) ) ;
#40634=EDGE_CURVE ( 'NONE', #90027, #53562, #84433, .T. ) ;
#40635=CARTESIAN_POINT ( 'NONE',  ( -110.2093792378191921, -25.29160350784524880, 5.585409231008217290 ) ) ;
#40637=CARTESIAN_POINT ( 'NONE',  ( -32.52287095715006160, -23.47596703998600631, 11.44779298504229459 ) ) ;
#40638=CARTESIAN_POINT ( 'NONE',  ( -69.33422667675866080, -25.12112739299269037, 7.112216829152949948 ) ) ;
#40639=CARTESIAN_POINT ( 'NONE',  ( 21.37280783159109276, 7.349196219051140844, -1.500000000000002220 ) ) ;
#40640=CARTESIAN_POINT ( 'NONE',  ( -88.88918693012686845, -25.23397913219354649, 6.409327625488847602 ) ) ;
#40642=CARTESIAN_POINT ( 'NONE',  ( -79.62713573843802806, -25.30166916552286693, 4.689104876704957015 ) ) ;
#40643=CARTESIAN_POINT ( 'NONE',  ( -31.48242477323742605, -24.51419770103156637, 9.386484678747187615 ) ) ;
#40644=CARTESIAN_POINT ( 'NONE',  ( 6.578723047037327909, -18.57437435983987584, 11.49999999999999645 ) ) ;
#40645=CARTESIAN_POINT ( 'NONE',  ( -93.55620429048339304, -23.48786465467241413, 11.44779295918253936 ) ) ;
#40646=FACE_OUTER_BOUND ( 'NONE', #29937, .T. ) ;
#40648=B_SPLINE_CURVE_WITH_KNOTS ( 'NONE', 3,
 ( #89, #49290, #78689, #87323 ),
 .UNSPECIFIED., .F., .F.,
 ( 4, 4 ),
 ( 0.1088347601982936758, 0.1098355072390591741 ),
 .UNSPECIFIED. ) ;
#40650=CARTESIAN_POINT ( 'NONE',  ( -89.52287095715006160, -24.64965694238407323, 8.947790433994196491 ) ) ;
#40652=DIRECTION ( 'NONE',  ( 0.000000000000000000, -0.9999999999976377785, -2.173523156925979128E-06 ) ) ;
#40653=CARTESIAN_POINT ( 'NONE',  ( -120.6228709571500417, -24.99132157543166954, 2.256160258750667502 ) ) ;
#40655=CARTESIAN_POINT ( 'NONE',  ( 2.412641546452875208, 19.58572291230954221, 11.49999999999998934 ) ) ;
#40658=AXIS2_PLACEMENT_3D ( 'NONE', #37697, #68657, #62544 ) ;
#40659=CARTESIAN_POINT ( 'NONE',  ( -19.21899500656021331, -6.280627263257740900, 11.49999999999999645 ) ) ;
#40660=CARTESIAN_POINT ( 'NONE',  ( -72.62287095715005592, -24.64898659630367916, 1.056161002820824368 ) ) ;
#40662=CARTESIAN_POINT ( 'NONE',  ( -110.6228709571500417, -24.52232992886363760, 0.6492154411906180256 ) ) ;
#40663=CARTESIAN_POINT ( 'NONE',  ( -69.48291834206632700, -25.28410036694619123, 5.733557524135145300 ) ) ;
#40665=DIRECTION ( 'NONE',  ( -1.000000000000000000, -3.773278334444167608E-23, -8.201307833595939069E-29 ) ) ;
#40666=CARTESIAN_POINT ( 'NONE',  ( -95.62287095715005592, -29.50250786944525672, 11.44777988621623166 ) ) ;
#40668=CARTESIAN_POINT ( 'NONE',  ( 14.90458806734895703, -13.33898509196910886, -1.500000000000002220 ) ) ;
#40670=DIRECTION ( 'NONE',  ( -0.000000000000000000, 2.173523156925979552E-06, -0.9999999999976378895 ) ) ;
#40671=CARTESIAN_POINT ( 'NONE',  ( -116.6251858524873342, -24.35071581493544102, 9.817618358456021710 ) ) ;
#40672=EDGE_LOOP ( 'NONE', ( #24833, #91755, #1154, #17614 ) ) ;
#40673=B_SPLINE_CURVE_WITH_KNOTS ( 'NONE', 3,
 ( #56750, #57743, #82060, #25776 ),
 .UNSPECIFIED., .F., .F.,
 ( 4, 4 ),
 ( 0.000000000000000000, 9.999999999998898659E-05 ),
 .UNSPECIFIED. ) ;
#40674=CARTESIAN_POINT ( 'NONE',  ( -69.86226847989213695, -25.12049686670126292, 2.832401160916445004 ) ) ;
#40675=CARTESIAN_POINT ( 'NONE',  ( -33.62287095715005592, -24.65952944569304250, 1.056160979905690356 ) ) ;
#40676=CARTESIAN_POINT ( 'NONE',  ( -92.62287095715005592, -24.64965695001469115, 8.947790433994180503 ) ) ;
#40677=CARTESIAN_POINT ( 'NONE',  ( -124.5895376238167103, -24.65952944569304961, 1.056160979905701902 ) ) ;
#40678=CARTESIAN_POINT ( 'NONE',  ( -51.69903695958453227, -25.31574265807444846, 4.034228563096281306 ) ) ;
#40680=EDGE_CURVE ( 'NONE', #24252, #58964, #68901, .T. ) ;
#40681=CARTESIAN_POINT ( 'NONE',  ( -49.54527677626192883, -25.24403278070153789, 3.779632570335008435 ) ) ;
#40682=ORIENTED_EDGE ( 'NONE', *, *, #92475, .T. ) ;
#40683=CARTESIAN_POINT ( 'NONE',  ( -6.898722100468609675, -19.10483383855023476, -1.500000000000002220 ) ) ;
#40685=CARTESIAN_POINT ( 'NONE',  ( -114.9228709571500673, -23.47593901973090169, -1.443836447538996426 ) ) ;
#40687=CARTESIAN_POINT ( 'NONE',  ( -107.5228709571500900, -24.35013146730204170, 9.818937971375099494 ) ) ;
#40690=CARTESIAN_POINT ( 'NONE',  ( -21.11812214938331422, 0.5215410354952813021, 11.49999999999999645 ) ) ;
#40691=CARTESIAN_POINT ( 'NONE',  ( -0.9539927174334467130, 22.11892580961223587, 11.49999999999998934 ) ) ;
#40693=CARTESIAN_POINT ( 'NONE',  ( -19.32567751138619982, -7.045664331180771178, 11.49999999999998934 ) ) ;
#40698=CARTESIAN_POINT ( 'NONE',  ( -70.52287095715007581, -23.47596703998600631, 11.44779298504228748 ) ) ;
#40700=ORIENTED_EDGE ( 'NONE', *, *, #39535, .T. ) ;
#40701=ORIENTED_EDGE ( 'NONE', *, *, #71603, .F. ) ;
#40702=CARTESIAN_POINT ( 'NONE',  ( -100.5228709571500616, -24.82558206586143612, 1.605769216559450152 ) ) ;
#40705=CARTESIAN_POINT ( 'NONE',  ( 3.345817365282868217, 20.41450801592841557, -1.500000000000002220 ) ) ;
#40706=CARTESIAN_POINT ( 'NONE',  ( -18.45943378446990835, 11.37049804852326140, 11.49999999999999645 ) ) ;
#40708=LINE ( 'NONE', #44213, #54793 ) ;
#40709=CARTESIAN_POINT ( 'NONE',  ( -110.9770695239891012, -25.13602867479627179, 2.978790624164922018 ) ) ;
#40710=CARTESIAN_POINT ( 'NONE',  ( 20.53814608839396527, -8.957171556794316203, -1.500000000000002220 ) ) ;
#40711=CARTESIAN_POINT ( 'NONE',  ( -92.62287095715005592, -23.47593901973091235, -1.443836447539002865 ) ) ;
#40712=CARTESIAN_POINT ( 'NONE',  ( -101.5228709571500758, -23.72773821059536203, 11.05748984161097148 ) ) ;
#40713=VERTEX_POINT ( 'NONE', #73601 ) ;
#40714=CARTESIAN_POINT ( 'NONE',  ( -54.62287095715005592, -29.50250786944525672, 11.44777988621624054 ) ) ;
#40716=CARTESIAN_POINT ( 'NONE',  ( -120.6228709571500417, -23.85229601348997619, 10.88205029486208275 ) ) ;
#40717=EDGE_LOOP ( 'NONE', ( #88449, #84113, #26394, #60311 ) ) ;
#40718=ORIENTED_EDGE ( 'NONE', *, *, #28753, .F. ) ;
#40719=CARTESIAN_POINT ( 'NONE',  ( -59.52287095715006160, -29.50250243563736774, 8.947779886222145151 ) ) ;
#40722=CARTESIAN_POINT ( 'NONE',  ( 4.903939382885006637, -20.63555827282145572, -1.500000000000002220 ) ) ;
#40724=CARTESIAN_POINT ( 'NONE',  ( -50.47485263706386149, -25.00158670708910691, 2.256160236439223254 ) ) ;
#40725=CARTESIAN_POINT ( 'NONE',  ( -20.50126671893153940, -7.481214725051755110, 11.49999999999998934 ) ) ;
#40726=CARTESIAN_POINT ( 'NONE',  ( -52.48645163059850915, -24.66019654487198665, 8.947790411086131712 ) ) ;
#40729=CARTESIAN_POINT ( 'NONE',  ( 21.83365961380331655, 0.8745889840297637052, -1.500000000000002220 ) ) ;
#40730=CARTESIAN_POINT ( 'NONE',  ( -30.57287095715005520, -25.30541082164580757, 5.278019199569442321 ) ) ;
#40733=CARTESIAN_POINT ( 'NONE',  ( -85.63004653390532894, -24.63419186844611275, 9.035850630976915099 ) ) ;
#40736=ORIENTED_EDGE ( 'NONE', *, *, #45034, .F. ) ;
#40737=ADVANCED_FACE ( 'NONE', ( #19300 ), #3106, .F. ) ;
#40738=CARTESIAN_POINT ( 'NONE',  ( -79.11611000704996854, -25.20074463982482982, 3.409327697717700278 ) ) ;
#40739=CARTESIAN_POINT ( 'NONE',  ( -82.54135565317993439, -24.65952944569304606, 1.056160979905703012 ) ) ;
#40740=B_SPLINE_CURVE_WITH_KNOTS ( 'NONE', 3,
 ( #82857, #13842, #97097, #29572 ),
 .UNSPECIFIED., .F., .F.,
 ( 4, 4 ),
 ( 0.000000000000000000, 9.999999999998897304E-05 ),
 .UNSPECIFIED. ) ;
#40741=CARTESIAN_POINT ( 'NONE',  ( -21.08860491664495029, 2.407354197416772035, -1.500000000000002220 ) ) ;
#40742=CARTESIAN_POINT ( 'NONE',  ( -125.5562042904833930, -25.00182538069145721, 7.747789668545099317 ) ) ;
#40743=EDGE_CURVE ( 'NONE', #36540, #52940, #85795, .T. ) ;
#40744=CARTESIAN_POINT ( 'NONE',  ( -81.62287095715005592, -29.50250786944525672, 11.44777988621623521 ) ) ;
#40746=CARTESIAN_POINT ( 'NONE',  ( -128.5895376238167103, -23.47593901973091235, -1.443836447538995760 ) ) ;
#40747=CARTESIAN_POINT ( 'NONE',  ( 11.07193147992585835, -15.93265361536492364, -1.500000000000002220 ) ) ;
#40748=CARTESIAN_POINT ( 'NONE',  ( -45.55047939234961518, -24.15503026093915651, -0.2815557561904415418 ) ) ;
#40750=CARTESIAN_POINT ( 'NONE',  ( -13.24781383850973349, 14.34467480260970795, 11.49999999999999645 ) ) ;
#40753=EDGE_CURVE ( 'NONE', #61052, #65701, #53103, .T. ) ;
#40754=EDGE_LOOP ( 'NONE', ( #43609, #36179, #81914, #61526 ) ) ;
#40755=CARTESIAN_POINT ( 'NONE',  ( -99.52287095715006160, -23.47596703998600631, 11.44779298504228215 ) ) ;
#40756=CARTESIAN_POINT ( 'NONE',  ( -32.62287095715004881, -23.48786465467240347, 11.44779295918255535 ) ) ;
#40757=B_SPLINE_CURVE_WITH_KNOTS ( 'NONE', 3,
 ( #34331, #72399, #42951, #10988 ),
 .UNSPECIFIED., .F., .F.,
 ( 4, 4 ),
 ( 0.000000000000000000, 9.999999999994735322E-05 ),
 .UNSPECIFIED. ) ;
#40759=CARTESIAN_POINT ( 'NONE',  ( -80.89908437845683409, -25.24813981080061609, 7.516074972019308298 ) ) ;
#40760=CARTESIAN_POINT ( 'NONE',  ( -18.24527198174902765, 7.358211898524878336, 11.49999999999998934 ) ) ;
#40761=ORIENTED_EDGE ( 'NONE', *, *, #100121, .T. ) ;
#40763=CARTESIAN_POINT ( 'NONE',  ( -63.62287095715004881, -29.50250786944525672, 11.44777988621623876 ) ) ;
#40764=CARTESIAN_POINT ( 'NONE',  ( 14.65057173600216345, 17.85730367728733725, -1.500000000000002220 ) ) ;
#40767=CARTESIAN_POINT ( 'NONE',  ( -90.52287095715009002, -24.51254535375846544, 9.355368624242132114 ) ) ;
#40768=CARTESIAN_POINT ( 'NONE',  ( -114.6228709571500559, -24.64898659630528854, 1.056161002820831474 ) ) ;
#40769=CARTESIAN_POINT ( 'NONE',  ( -76.52287095715011844, -23.48783264082477373, -1.443836473390087694 ) ) ;
#40770=CARTESIAN_POINT ( 'NONE',  ( -119.5228709571500900, -23.94994826722565406, -0.6494450866342709183 ) ) ;
#40773=CARTESIAN_POINT ( 'NONE',  ( -73.52287095715006160, -23.73934037231756733, 11.05740245334329153 ) ) ;
#40774=CARTESIAN_POINT ( 'NONE',  ( -111.3439979973304332, -25.29779330784409552, 4.101024009883487587 ) ) ;
#40775=CARTESIAN_POINT ( 'NONE',  ( -18.10700488460823721, -8.296952762055457953, 11.49999999999998934 ) ) ;
#40776=CARTESIAN_POINT ( 'NONE',  ( -75.62935365942843191, -24.73531770709095312, 8.716586749053512051 ) ) ;
#40777=CARTESIAN_POINT ( 'NONE',  ( 16.83370257367741019, -10.51912618480096206, -1.500000000000002220 ) ) ;
#40778=ORIENTED_EDGE ( 'NONE', *, *, #19841, .T. ) ;
#40780=EDGE_CURVE ( 'NONE', #39121, #43756, #42667, .T. ) ;
#40783=CARTESIAN_POINT ( 'NONE',  ( -125.5228709571500616, -24.51163499207176244, 0.6490370598554348058 ) ) ;
#40784=CARTESIAN_POINT ( 'NONE',  ( -92.62287095715005592, -29.50247984919015209, -1.443849546365051806 ) ) ;
#40785=CARTESIAN_POINT ( 'NONE',  ( 11.56195852851363526, -17.29799701895051811, 11.49999999999999645 ) ) ;
#40787=EDGE_CURVE ( 'NONE', #12406, #84010, #89323, .T. ) ;
#40788=CARTESIAN_POINT ( 'NONE',  ( -106.6264179404533508, -24.34968618360933945, 0.1864209137778878034 ) ) ;
#40789=CARTESIAN_POINT ( 'NONE',  ( -4.374245501123523283, 22.36648047097513725, 11.49999999999999645 ) ) ;
#40791=CARTESIAN_POINT ( 'NONE',  ( -69.54085705957912467, -24.51314013834315375, 0.6176544820404143987 ) ) ;
#40792=CARTESIAN_POINT ( 'NONE',  ( -92.52287095715006160, -23.72773821059536914, 11.05748984161097326 ) ) ;
#40794=CARTESIAN_POINT ( 'NONE',  ( -10.81679630089563915, -17.07601267366916886, -1.500000000000002220 ) ) ;
#40795=CARTESIAN_POINT ( 'NONE',  ( -33.62287095715005592, -29.50248528299804818, 1.056150453629029817 ) ) ;
#40798=CARTESIAN_POINT ( 'NONE',  ( -105.5228709571500616, -29.50248789122583659, 2.256150453626215580 ) ) ;
#40800=CARTESIAN_POINT ( 'NONE',  ( 4.555139465550277933, 19.45931829295258453, -1.500000000000002220 ) ) ;
#40802=CARTESIAN_POINT ( 'NONE',  ( 19.98859412959824411, 6.261702723725245612, 11.49999999999999645 ) ) ;
#40804=CARTESIAN_POINT ( 'NONE',  ( -79.55620429048340725, -24.64965694238574656, 8.947790433994196491 ) ) ;
#40805=CARTESIAN_POINT ( 'NONE',  ( 20.91424602935089894, 6.983905699820807556, 11.49999999999998934 ) ) ;
#40806=EDGE_CURVE ( 'NONE', #22913, #79917, #49779, .T. ) ;
#40808=EDGE_LOOP ( 'NONE', ( #10312, #53689, #75135, #27266 ) ) ;
#40810=LINE ( 'NONE', #18970, #69465 ) ;
#40811=DIRECTION ( 'NONE',  ( -1.000000000000000000, -3.773278334444166432E-23, -8.201307841325785021E-29 ) ) ;
#40812=CARTESIAN_POINT ( 'NONE',  ( -72.50263257038113807, -24.34968618360933590, 0.1864209137778795600 ) ) ;
#40815=EDGE_LOOP ( 'NONE', ( #71339, #95386, #82385, #88747 ) ) ;
#40817=CARTESIAN_POINT ( 'NONE',  ( -79.22287095715010707, -23.47593901973090524, -1.443836447538997536 ) ) ;
#40818=CARTESIAN_POINT ( 'NONE',  ( -85.52287095715009002, -23.47593901973090524, -1.443836447538996648 ) ) ;
#40819=CARTESIAN_POINT ( 'NONE',  ( -122.5895376238167387, -23.48786465467242124, 11.44779295918253759 ) ) ;
#40820=CARTESIAN_POINT ( 'NONE',  ( 16.43461662053371697, -12.34185696772103391, -1.500000000000002220 ) ) ;
#40822=CARTESIAN_POINT ( 'NONE',  ( -99.35299720551914504, -25.27660924118455910, 5.844709891833338666 ) ) ;
#40823=EDGE_CURVE ( 'NONE', #25493, #85607, #14435, .T. ) ;
#40825=CARTESIAN_POINT ( 'NONE',  ( -96.62287095715005592, -24.66019654487199730, 8.947790411086124607 ) ) ;
#40826=CARTESIAN_POINT ( 'NONE',  ( -7.907391756136429528, -20.87048397725295956, 11.49999999999998934 ) ) ;
#40827=CARTESIAN_POINT ( 'NONE',  ( -81.62287095715005592, -24.50216790748099882, 0.6166512839513619282 ) ) ;
#40828=DIRECTION ( 'NONE',  ( -3.773278334444166432E-23, 1.000000000000000000, 0.000000000000000000 ) ) ;
#40830=FACE_OUTER_BOUND ( 'NONE', #77226, .T. ) ;
#40831=CARTESIAN_POINT ( 'NONE',  ( -65.62287095715005592, -24.99132157543084176, 2.256160258750667502 ) ) ;
#40832=CARTESIAN_POINT ( 'NONE',  ( -9.832896139050584239, -18.40278743011522877, -1.500000000000002220 ) ) ;
#40836=ORIENTED_EDGE ( 'NONE', *, *, #13274, .T. ) ;
#40837=ORIENTED_EDGE ( 'NONE', *, *, #97082, .T. ) ;
#40838=CARTESIAN_POINT ( 'NONE',  ( -58.87764846858842560, -29.50248939449842922, 2.947779886236309377 ) ) ;
#40839=CARTESIAN_POINT ( 'NONE',  ( -2.129267666952235682, 20.92775224702969439, -1.500000000000002220 ) ) ;
#40841=DIRECTION ( 'NONE',  ( 0.000000000000000000, -0.9999999999976377785, -2.173523156925979128E-06 ) ) ;
#40843=CARTESIAN_POINT ( 'NONE',  ( -111.6228709571500559, -23.47593901973091235, -1.443836447538999312 ) ) ;
#40844=CARTESIAN_POINT ( 'NONE',  ( -86.55119192925248228, -24.15620529776628445, 10.23563542870660292 ) ) ;
#40845=ADVANCED_FACE ( 'NONE', ( #27428 ), #43159, .T. ) ;
#40846=CARTESIAN_POINT ( 'NONE',  ( -49.62287095715005592, -24.64898659630528499, 1.056161002820821038 ) ) ;
#40847=CARTESIAN_POINT ( 'NONE',  ( 3.708801897538985148, -21.39311272803122321, -1.500000000000002220 ) ) ;
#40850=CARTESIAN_POINT ( 'NONE',  ( -10.57539506955483333, 19.50334513348995813, 11.49999999999999645 ) ) ;
#40853=CARTESIAN_POINT ( 'NONE',  ( -71.30260502180048832, -25.25163510122737165, 6.148193815974848597 ) ) ;
#40854=VERTEX_POINT ( 'NONE', #36028 ) ;
#40855=CARTESIAN_POINT ( 'NONE',  ( 14.05383982582471170, -17.77673030755399708, -1.500000000000002220 ) ) ;
#40856=B_SPLINE_CURVE_WITH_KNOTS ( 'NONE', 3,
 ( #22292, #85715, #8088, #69985, #84704, #46662 ),
 .UNSPECIFIED., .F., .F.,
 ( 4, 2, 4 ),
 ( 1.570755371634052715E-05, 0.001396183895866088187, 0.002776660238015835579 ),
 .UNSPECIFIED. ) ;
#40859=B_SPLINE_CURVE_WITH_KNOTS ( 'NONE', 3,
 ( #5213, #12313, #98046, #28541 ),
 .UNSPECIFIED., .F., .F.,
 ( 4, 4 ),
 ( 0.000000000000000000, 9.999999999998897304E-05 ),
 .UNSPECIFIED. ) ;
#40863=CARTESIAN_POINT ( 'NONE',  ( -101.5228709571500758, -23.48786465467241769, 11.44779295918254114 ) ) ;
#40864=EDGE_CURVE ( 'NONE', #24496, #48489, #99061, .T. ) ;
#40865=CARTESIAN_POINT ( 'NONE',  ( 13.10547390533899836, 15.29217475743441312, 11.49999999999998934 ) ) ;
#40866=EDGE_CURVE ( 'NONE', #4006, #69692, #75078, .T. ) ;
#40867=CARTESIAN_POINT ( 'NONE',  ( -105.5228709571501042, -23.48783264082477018, -1.443836473390085917 ) ) ;
#40869=CARTESIAN_POINT ( 'NONE',  ( -130.5728709571500588, -24.64113408559786933, 0.7260449476895605159 ) ) ;
#40870=CARTESIAN_POINT ( 'NONE',  ( 1.438201247614206757, 22.34484416265529916, -1.500000000000002220 ) ) ;
#40871=EDGE_CURVE ( 'NONE', #21106, #25496, #21620, .T. ) ;
#40873=ORIENTED_EDGE ( 'NONE', *, *, #83577, .F. ) ;
#40874=CARTESIAN_POINT ( 'NONE',  ( -89.40841769935767047, -25.06732983082694943, 7.447789526168953955 ) ) ;
#40875=CARTESIAN_POINT ( 'NONE',  ( -94.52217260166209201, -23.48786465467241058, 11.44779295918254469 ) ) ;
#40879=CARTESIAN_POINT ( 'NONE',  ( -97.24912498359577739, -24.57143472585066490, 0.8294870405985540485 ) ) ;
#40880=CARTESIAN_POINT ( 'NONE',  ( -6.365771329251782795, -18.49506561991874065, 11.49999999999998934 ) ) ;
#40881=B_SPLINE_SURFACE_WITH_KNOTS ( 'NONE', 3, 1, ( 
 ( #51908, #29052 ),
 ( #61016, #12822 ),
 ( #91949, #43793 ),
 ( #83838, #5223 ),
 ( #6712, #98054 ),
 ( #59519, #98555 ),
 ( #37665, #5719 ),
 ( #90456, #36668 ),
 ( #83337, #13817 ),
 ( #40678, #2126 ),
 ( #93440, #16325 ) ),
 .UNSPECIFIED., .F., .F., .F.,
 ( 4, 1, 1, 1, 1, 1, 1, 1, 4 ),
 ( 2, 2 ),
 ( 0.000000000000000000, 0.1458600603916643534, 0.2824259030758165534, 0.4108504003575531582, 0.5350294213479291905, 0.6547010781259405832, 0.7701334325965021321, 0.8845558441988605747, 1.000000000000000000 ),
 ( 0.000000000000000000, 1.000000000000000000 ),
 .UNSPECIFIED. ) ;
#40882=CARTESIAN_POINT ( 'NONE',  ( -46.59984531427831911, -23.96119346886879953, -0.6495511937832144644 ) ) ;
#40883=VERTEX_POINT ( 'NONE', #13675 ) ;
#40884=CARTESIAN_POINT ( 'NONE',  ( 21.22668844964908885, 3.412186807495566132, -1.500000000000002220 ) ) ;
#40885=CARTESIAN_POINT ( 'NONE',  ( -128.5561025698958701, -23.73766607897671932, -1.055555164236423149 ) ) ;
#40889=CARTESIAN_POINT ( 'NONE',  ( 12.20170062390598709, -19.39347807479101249, -1.500000000000002220 ) ) ;
#40891=CARTESIAN_POINT ( 'NONE',  ( -31.55620429048339304, -24.66019654487198309, 8.947790411086138818 ) ) ;
#40893=CARTESIAN_POINT ( 'NONE',  ( -17.82723130383223165, -9.322377578706960932, 11.49999999999999645 ) ) ;
#40895=LINE ( 'NONE', #1843, #48434 ) ;
#40897=PLANE ( 'NONE',  #84648 ) ;
#40898=CARTESIAN_POINT ( 'NONE',  ( -129.5228709571500758, -29.50247984919015209, -1.443849546365044922 ) ) ;
#40900=CARTESIAN_POINT ( 'NONE',  ( -11.71124675921804403, 15.99993322257668282, -1.500000000000002220 ) ) ;
#40901=CARTESIAN_POINT ( 'NONE',  ( 20.57166443188586769, -7.073620337204646447, -1.500000000000002220 ) ) ;
#40903=CARTESIAN_POINT ( 'NONE',  ( 16.84789977498956404, 10.09486508543780481, -1.500000000000002220 ) ) ;
#40908=DIRECTION ( 'NONE',  ( -1.000000000000000000, -3.773278334444166432E-23, -8.201307841325785021E-29 ) ) ;
#40910=CARTESIAN_POINT ( 'NONE',  ( 19.85418835109896563, -5.301297255791479479, 11.49999999999999645 ) ) ;
#40912=FACE_OUTER_BOUND ( 'NONE', #3646, .T. ) ;
#40913=CARTESIAN_POINT ( 'NONE',  ( -22.62345309801473547, -0.4825844212548152656, 11.49999999999999645 ) ) ;
#40915=ORIENTED_EDGE ( 'NONE', *, *, #92835, .T. ) ;
#40916=CARTESIAN_POINT ( 'NONE',  ( -115.5228709571500758, -25.00182538069145721, 7.747789668545101094 ) ) ;
#40919=CARTESIAN_POINT ( 'NONE',  ( -56.52287095715004739, -23.73907113216989018, -1.053371485793253459 ) ) ;
#40920=CARTESIAN_POINT ( 'NONE',  ( -39.62287095715005592, -23.47593901973091235, -1.443836447539011525 ) ) ;
#40921=B_SPLINE_CURVE_WITH_KNOTS ( 'NONE', 3,
 ( #84603, #70893, #47056, #94207, #70383, #38928 ),
 .UNSPECIFIED., .F., .F.,
 ( 4, 2, 4 ),
 ( 0.000000000000000000, 0.001380901958385379220, 0.002761803916770758441 ),
 .UNSPECIFIED. ) ;
#40922=CARTESIAN_POINT ( 'NONE',  ( -26.59548113855183615, -24.61460036469634005, 7.895922928448310785 ) ) ;
#40923=CARTESIAN_POINT ( 'NONE',  ( -28.52287095715006515, -23.57592831105002773, 11.05752276746862073 ) ) ;
#40924=ORIENTED_EDGE ( 'NONE', *, *, #97141, .T. ) ;
#40926=CARTESIAN_POINT ( 'NONE',  ( -79.80213995901898727, -25.31596255503136916, 5.120505554222577693 ) ) ;
#40927=CARTESIAN_POINT ( 'NONE',  ( -12.33899560737860313, 19.21699747222852395, 11.49999999999998934 ) ) ;
#40928=CARTESIAN_POINT ( 'NONE',  ( -110.8640811366819179, -25.20146121768474501, 3.413985529804576480 ) ) ;
#40930=CARTESIAN_POINT ( 'NONE',  ( -63.53934691136210944, -24.51419770103156992, 9.386484678747175181 ) ) ;
#40932=CARTESIAN_POINT ( 'NONE',  ( 17.90692129536829924, 13.62026984716248101, 11.49999999999999645 ) ) ;
#40934=CARTESIAN_POINT ( 'NONE',  ( -33.55620429048340014, -23.48786465467240347, 11.44779295918255713 ) ) ;
#40935=CARTESIAN_POINT ( 'NONE',  ( -16.59477544326466969, -14.39948450415919723, -1.500000000000002220 ) ) ;
#40936=CARTESIAN_POINT ( 'NONE',  ( -127.1722404401672577, -25.37154127157531391, 4.079011290487088992 ) ) ;
#40937=EDGE_CURVE ( 'NONE', #49847, #3669, #76077, .T. ) ;
#40939=CARTESIAN_POINT ( 'NONE',  ( -56.52287095715006870, -23.48786465467241058, 11.44779295918254824 ) ) ;
#40940=VECTOR ( 'NONE', #14538, 1000.000000000000114 ) ;
#40942=DIRECTION ( 'NONE',  ( -0.000000000000000000, 2.173523156925979552E-06, -0.9999999999976378895 ) ) ;
#40944=ORIENTED_EDGE ( 'NONE', *, *, #52810, .F. ) ;
#40945=CARTESIAN_POINT ( 'NONE',  ( 18.57849760351508195, 8.651319581928444080, 11.49999999999998934 ) ) ;
#40946=ORIENTED_EDGE ( 'NONE', *, *, #41009, .F. ) ;
#40947=ORIENTED_EDGE ( 'NONE', *, *, #74359, .T. ) ;
#40948=ORIENTED_EDGE ( 'NONE', *, *, #90786, .T. ) ;
#40950=LINE ( 'NONE', #10999, #43675 ) ;
#40951=CARTESIAN_POINT ( 'NONE',  ( -0.07435467474217070938, 23.09247799282200475, 11.49999999999998934 ) ) ;
#40953=CARTESIAN_POINT ( 'NONE',  ( 9.809556900635294951, 17.81656380412256269, -1.500000000000002220 ) ) ;
#40954=ORIENTED_EDGE ( 'NONE', *, *, #4427, .T. ) ;
#40955=EDGE_CURVE ( 'NONE', #2649, #28831, #94231, .T. ) ;
#40956=DIRECTION ( 'NONE',  ( -3.773278334453079618E-23, 0.9999999999976377785, 2.173523156925979975E-06 ) ) ;
#40958=CARTESIAN_POINT ( 'NONE',  ( -29.62375005554824980, -24.58464305241082215, 8.947790440257527678 ) ) ;
#40959=ADVANCED_FACE ( 'NONE', ( #61379 ), #97914, .F. ) ;
#40960=CARTESIAN_POINT ( 'NONE',  ( -101.4685450411434573, -25.22743938310598466, 6.465526456246802667 ) ) ;
#40962=CARTESIAN_POINT ( 'NONE',  ( -2.508422780830330989, 21.39056295969660582, 11.49999999999999645 ) ) ;
#40963=EDGE_LOOP ( 'NONE', ( #72929, #72274, #41363, #88597 ) ) ;
#40964=CARTESIAN_POINT ( 'NONE',  ( -29.13856514152708499, -24.76881155732394646, 3.662309959797942049 ) ) ;
#40965=CARTESIAN_POINT ( 'NONE',  ( -49.74369414166532977, -25.26385844215123910, 4.940878041311237645 ) ) ;
#40966=EDGE_CURVE ( 'NONE', #84539, #93818, #93149, .T. ) ;
#40968=CARTESIAN_POINT ( 'NONE',  ( -15.22196369898608737, 14.14466773073655581, -1.500000000000002220 ) ) ;
#40970=CARTESIAN_POINT ( 'NONE',  ( -91.55620429048340725, -24.64898659630528854, 1.056161002820825034 ) ) ;
#40971=ORIENTED_EDGE ( 'NONE', *, *, #93990, .F. ) ;
#40972=VECTOR ( 'NONE', #29267, 1000.000000000000114 ) ;
#40973=B_SPLINE_SURFACE_WITH_KNOTS ( 'NONE', 3, 1, ( 
 ( #55635, #17050 ),
 ( #62752, #9437 ),
 ( #16539, #85058 ),
 ( #23653, #76935 ),
 ( #328, #55131 ),
 ( #39890, #78942 ),
 ( #93669, #38388 ),
 ( #48017, #86065 ),
 ( #24161, #47515 ),
 ( #7433, #69341 ),
 ( #85560, #78440 ),
 ( #54133, #71353 ),
 ( #15044, #92667 ),
 ( #8941, #30778 ),
 ( #15545, #100260 ),
 ( #1842, #54626 ),
 ( #40400, #70850 ),
 ( #16043, #61748 ),
 ( #47011, #59875 ) ),
 .UNSPECIFIED., .F., .F., .F.,
 ( 4, 1, 1, 1, 1, 1, 1, 1, 1, 1, 1, 1, 1, 1, 1, 1, 4 ),
 ( 2, 2 ),
 ( 0.000000000000000000, 0.06580764581069505070, 0.1293942736680568084, 0.1908940606321889999, 0.2512810689298332067, 0.3108149644652716814, 0.3703709874482468689, 0.4307682625897272244, 0.4928812506175027641, 0.5551039481552511035, 0.6160670509938424022, 0.6772560331746547702, 0.7382598051991177135, 0.8007621343762953980, 0.8647775815744849215, 0.9310452949994038052, 1.000000000000000000 ),
 ( 0.000000000000000000, 1.000000000000000000 ),
 .UNSPECIFIED. ) ;
#40975=CARTESIAN_POINT ( 'NONE',  ( -51.92629526020853348, -25.26139929061960387, 6.040166309471107553 ) ) ;
#40978=PLANE ( 'NONE',  #91515 ) ;
#40979=CARTESIAN_POINT ( 'NONE',  ( -68.62287095715004170, -24.66019654487199020, 8.947790411086131712 ) ) ;
#40980=CARTESIAN_POINT ( 'NONE',  ( -29.76928132860276577, -25.21455316847251282, 4.017376845980065170 ) ) ;
#40981=ADVANCED_FACE ( 'NONE', ( #45152 ), #6575, .F. ) ;
#40982=ADVANCED_FACE ( 'NONE', ( #60876 ), #59883, .T. ) ;
#40983=CARTESIAN_POINT ( 'NONE',  ( 12.33731239738771102, -18.22686410513083288, 11.49999999999999645 ) ) ;
#40984=EDGE_LOOP ( 'NONE', ( #76149, #23204, #41205, #1515 ) ) ;
#40985=CARTESIAN_POINT ( 'NONE',  ( -103.5131199472542676, -24.34968618360933945, 0.1864209137778842229 ) ) ;
#40987=CARTESIAN_POINT ( 'NONE',  ( -21.83012794225054165, -5.757306806698124113, 11.49999999999998934 ) ) ;
#40990=VECTOR ( 'NONE', #26552, 1000.000000000000114 ) ;
#40991=EDGE_LOOP ( 'NONE', ( #30248, #55890, #19408, #46474 ) ) ;
#40994=ADVANCED_FACE ( 'NONE', ( #9577 ), #9075, .T. ) ;
#40995=LINE ( 'NONE', #71952, #95937 ) ;
#40996=ORIENTED_EDGE ( 'NONE', *, *, #42191, .F. ) ;
#40997=CARTESIAN_POINT ( 'NONE',  ( -0.2625952501129409367, 21.13516572482953748, -1.500000000000002220 ) ) ;
#40998=CARTESIAN_POINT ( 'NONE',  ( -34.62287095715006302, -24.51387760970723662, 9.387446482453425389 ) ) ;
#40999=CARTESIAN_POINT ( 'NONE',  ( -51.93149462243456327, -25.26040815178494725, 6.174051125736514045 ) ) ;
#41001=CARTESIAN_POINT ( 'NONE',  ( -80.62287095715004170, -25.00182538069145721, 7.747789668545097541 ) ) ;
#41002=CARTESIAN_POINT ( 'NONE',  ( -21.98633505697190671, -3.258044352128648846, -1.500000000000002220 ) ) ;
#41008=CARTESIAN_POINT ( 'NONE',  ( 18.72033823704212097, 5.060218808788302880, 11.49999999999999645 ) ) ;
#41009=EDGE_CURVE ( 'NONE', #36561, #6243, #37458, .T. ) ;
#41010=CARTESIAN_POINT ( 'NONE',  ( -40.89642461179924737, -25.12242866868528068, 2.899885291263534892 ) ) ;
#41011=CARTESIAN_POINT ( 'NONE',  ( -33.62287095715005592, -23.72773821059535493, 11.05748984161097503 ) ) ;
#41013=ADVANCED_FACE ( 'NONE', ( #55771 ), #16683, .F. ) ;
#41014=CARTESIAN_POINT ( 'NONE',  ( -16.97169330436246781, 9.548981535075045102, -1.500000000000002220 ) ) ;
#41016=CARTESIAN_POINT ( 'NONE',  ( 21.20698605602738951, -2.876969938318672870, 11.49999999999998934 ) ) ;
#41017=CARTESIAN_POINT ( 'NONE',  ( -56.62287095715005592, -23.47593901973091235, -1.443836447539007972 ) ) ;
#41018=CARTESIAN_POINT ( 'NONE',  ( -60.54474933874992360, -24.40133493613624083, 9.663955038888266458 ) ) ;
#41019=CARTESIAN_POINT ( 'NONE',  ( -51.54738905035295460, -24.15543982623907127, -0.2315651400026664530 ) ) ;
#41020=CARTESIAN_POINT ( 'NONE',  ( -77.59611061849884095, -23.96119346886880663, -0.6495511937832126881 ) ) ;
#41021=CARTESIAN_POINT ( 'NONE',  ( -21.15473383059569557, 8.456223909384457116, -1.500000000000002220 ) ) ;
#41022=VECTOR ( 'NONE', #92047, 1000.000000000000114 ) ;
#41023=EDGE_CURVE ( 'NONE', #73483, #71054, #47168, .T. ) ;
#41024=CARTESIAN_POINT ( 'NONE',  ( -106.5500282929658482, -24.51419770103158768, 9.386484678747164523 ) ) ;
#41026=CARTESIAN_POINT ( 'NONE',  ( 1.158388978951967463, 19.79969207489630634, 11.49999999999999645 ) ) ;
#41027=CARTESIAN_POINT ( 'NONE',  ( -123.5890674397278985, -24.51419770103158768, 9.386484678747160970 ) ) ;
#41028=VECTOR ( 'NONE', #51727, 1000.000000000000114 ) ;
#41029=CARTESIAN_POINT ( 'NONE',  ( -128.5228709571500758, -24.64965694238575722, 8.947790433994189385 ) ) ;
#41030=CARTESIAN_POINT ( 'NONE',  ( -100.4326965455114902, -25.19502912051678578, 3.293943094755625633 ) ) ;
#41031=VERTEX_POINT ( 'NONE', #24302 ) ;
#41032=DIRECTION ( 'NONE',  ( 0.000000000000000000, 0.9999999999976377785, 2.173523156925979128E-06 ) ) ;
#41033=CARTESIAN_POINT ( 'NONE',  ( -31.80982380344445204, -25.31558585043574183, 4.997857581739419075 ) ) ;
#41034=FACE_OUTER_BOUND ( 'NONE', #56848, .T. ) ;
#41035=CARTESIAN_POINT ( 'NONE',  ( 7.679218611123722837, 20.28660689097963399, 11.49999999999998934 ) ) ;
#41036=CARTESIAN_POINT ( 'NONE',  ( -124.6228709571500559, -29.50247984919015209, -1.443849546365046699 ) ) ;
#41037=CARTESIAN_POINT ( 'NONE',  ( -2.678125609936932605, 19.29598960679622976, -1.500000000000002220 ) ) ;
#41038=FACE_OUTER_BOUND ( 'NONE', #30245, .T. ) ;
#41040=CARTESIAN_POINT ( 'NONE',  ( -15.93830457579706739, -12.76012858937699335, 11.49999999999999645 ) ) ;
#41041=CARTESIAN_POINT ( 'NONE',  ( -49.55620429048338593, -23.47596703998600276, 11.44779298504227505 ) ) ;
#41043=ORIENTED_EDGE ( 'NONE', *, *, #4427, .F. ) ;
#41044=CARTESIAN_POINT ( 'NONE',  ( -37.52287095715006870, -23.48786465467240347, 11.44779295918255180 ) ) ;
#41047=PLANE ( 'NONE',  #24672 ) ;
#41049=CARTESIAN_POINT ( 'NONE',  ( -93.62287095715005592, -29.50247984919015209, -1.443849546365051806 ) ) ;
#41051=ORIENTED_EDGE ( 'NONE', *, *, #33075, .F. ) ;
#41052=CARTESIAN_POINT ( 'NONE',  ( -66.63617261146598025, -24.15620529776628089, 10.23563542870660470 ) ) ;
#41053=CARTESIAN_POINT ( 'NONE',  ( -22.63010559926462051, 4.001702944626347680, 11.49999999999999645 ) ) ;
#41054=CARTESIAN_POINT ( 'NONE',  ( -7.854035805165779927, 21.33931789143995417, 11.49999999999998934 ) ) ;
#41055=CARTESIAN_POINT ( 'NONE',  ( -110.5509673167211560, -24.63419186844610920, 9.035850630976920428 ) ) ;
#41056=AXIS2_PLACEMENT_3D ( 'NONE', #9704, #71613, #2109 ) ;
#41059=CARTESIAN_POINT ( 'NONE',  ( -82.52287095715001897, -23.48783264083388289, -1.443836473375923690 ) ) ;
#41060=CARTESIAN_POINT ( 'NONE',  ( -11.13288495942205536, 18.84158392345546318, 11.49999999999998934 ) ) ;
#41061=FACE_OUTER_BOUND ( 'NONE', #14131, .T. ) ;
#41062=EDGE_CURVE ( 'NONE', #36448, #48203, #32921, .T. ) ;
#41063=CARTESIAN_POINT ( 'NONE',  ( -49.68550546162367709, -25.31558437716839904, 4.971218732387883144 ) ) ;
#41065=CARTESIAN_POINT ( 'NONE',  ( -39.92287095715006018, -23.47593901973090169, -1.443836447538997980 ) ) ;
#41066=ORIENTED_EDGE ( 'NONE', *, *, #32972, .T. ) ;
#41067=ADVANCED_FACE ( 'NONE', ( #23794 ), #87892, .T. ) ;
#41068=CARTESIAN_POINT ( 'NONE',  ( -20.33632446988539400, 1.880062042347348195, -1.500000000000002220 ) ) ;
#41069=VERTEX_POINT ( 'NONE', #64399 ) ;
#41070=EDGE_LOOP ( 'NONE', ( #57401, #7595, #15319, #60491 ) ) ;
#41071=CARTESIAN_POINT ( 'NONE',  ( 22.26416322464526232, -5.798680748638591176, -1.500000000000002220 ) ) ;
#41074=VERTEX_POINT ( 'NONE', #49162 ) ;
#41078=ADVANCED_FACE ( 'NONE', ( #41038 ), #89702, .F. ) ;
#41080=AXIS2_PLACEMENT_3D ( 'NONE', #11465, #18571, #89093 ) ;
#41081=CARTESIAN_POINT ( 'NONE',  ( -35.52287095715006870, -24.99156044556120193, 7.747789690856173195 ) ) ;
#41083=CARTESIAN_POINT ( 'NONE',  ( -16.81368161134402683, 13.12552177539105358, 11.49999999999999645 ) ) ;
#41086=ORIENTED_EDGE ( 'NONE', *, *, #14028, .T. ) ;
#41087=CARTESIAN_POINT ( 'NONE',  ( -11.95080204275630464, 18.75100984808165094, 11.49999999999998934 ) ) ;
#41088=CARTESIAN_POINT ( 'NONE',  ( 18.87225196054570020, 8.368929400942139551, 11.49999999999998934 ) ) ;
#41090=ORIENTED_EDGE ( 'NONE', *, *, #72506, .F. ) ;
#41092=CARTESIAN_POINT ( 'NONE',  ( -95.56281998239499842, -23.48786465467241058, 11.44779295918254469 ) ) ;
#41093=VERTEX_POINT ( 'NONE', #42543 ) ;
#41094=CARTESIAN_POINT ( 'NONE',  ( -79.58953762381672448, -23.48786465467241058, 11.44779295918254469 ) ) ;
#41097=CARTESIAN_POINT ( 'NONE',  ( -58.52207410937929666, -23.48786465467241413, 11.44779295918254647 ) ) ;
#41099=CARTESIAN_POINT ( 'NONE',  ( 8.688630223215852766, -18.96179456382524364, -1.500000000000002220 ) ) ;
#41101=CARTESIAN_POINT ( 'NONE',  ( -21.47987282208850601, -4.139150239982721580, 11.49999999999999645 ) ) ;
#41102=CARTESIAN_POINT ( 'NONE',  ( -26.64126777428346315, -24.89279892862556665, 7.094643926469543338 ) ) ;
#41103=LINE ( 'NONE', #72058, #27269 ) ;
#41104=CARTESIAN_POINT ( 'NONE',  ( 21.70358988458699301, 5.938112137899119070, -1.500000000000002220 ) ) ;
#41105=CARTESIAN_POINT ( 'NONE',  ( 0.8369575198195864374, -20.89415947959451003, 11.49999999999998934 ) ) ;
#41106=CARTESIAN_POINT ( 'NONE',  ( -38.54597331675388716, -24.15543982623907127, -0.2315651400026569606 ) ) ;
#41107=CARTESIAN_POINT ( 'NONE',  ( -44.52287095715006160, -23.47596703998600631, 11.44779298504229281 ) ) ;
#41110=VERTEX_POINT ( 'NONE', #65891 ) ;
#41111=EDGE_LOOP ( 'NONE', ( #54200, #68771, #92714, #34950 ) ) ;
#41112=ORIENTED_EDGE ( 'NONE', *, *, #13517, .T. ) ;
#41113=CARTESIAN_POINT ( 'NONE',  ( -99.29687923781919778, -25.26221111348665005, 6.149712179509984722 ) ) ;
#41114=ORIENTED_EDGE ( 'NONE', *, *, #64057, .T. ) ;
#41115=CARTESIAN_POINT ( 'NONE',  ( 20.27498964588844643, 6.839650151297337999, -1.500000000000002220 ) ) ;
#41116=CARTESIAN_POINT ( 'NONE',  ( 8.126467401150291536, 20.86698325809501497, 11.49999999999999645 ) ) ;
#41117=EDGE_LOOP ( 'NONE', ( #14715, #8006, #11003, #46558 ) ) ;
#41118=CARTESIAN_POINT ( 'NONE',  ( -59.52287095715004028, -24.34917612406836795, 0.1852690917426535466 ) ) ;
#41119=CARTESIAN_POINT ( 'NONE',  ( -17.44821286160079410, -11.81026508430653088, 11.49999999999998934 ) ) ;
#41120=CARTESIAN_POINT ( 'NONE',  ( -61.52287095715007581, -23.47593901973090169, -1.443836447538997092 ) ) ;
#41121=CARTESIAN_POINT ( 'NONE',  ( -1.646307629438301667, 19.86461321233117872, -1.500000000000002220 ) ) ;
#41122=CARTESIAN_POINT ( 'NONE',  ( -50.62889347931399442, -24.83644354573578283, 8.397322867130100121 ) ) ;
#41123=B_SPLINE_CURVE_WITH_KNOTS ( 'NONE', 3,
 ( #9690, #93917, #64008, #56388, #24409, #17808, #55376, #86311 ),
 .UNSPECIFIED., .F., .F.,
 ( 4, 2, 2, 4 ),
 ( 0.000000000000000000, 0.002001098010032691023, 0.003001647015049036318, 0.004002196020065382047 ),
 .UNSPECIFIED. ) ;
#41124=CARTESIAN_POINT ( 'NONE',  ( -80.39981004835770761, -25.29534345565997100, 4.506608245854094363 ) ) ;
#41125=CARTESIAN_POINT ( 'NONE',  ( -20.87105610827876134, -7.033761084331515256, -1.500000000000002220 ) ) ;
#41127=CARTESIAN_POINT ( 'NONE',  ( -116.6298663670893632, -23.48783264082478439, -1.443836473390061936 ) ) ;
#41130=CARTESIAN_POINT ( 'NONE',  ( -78.62287095715007013, -24.51387760970723662, 9.387446482453411178 ) ) ;
#41131=EDGE_CURVE ( 'NONE', #37466, #75118, #49508, .T. ) ;
#41132=CARTESIAN_POINT ( 'NONE',  ( -26.95579990879923926, -24.88473778148743065, 7.214475432169975555 ) ) ;
#41133=B_SPLINE_CURVE_WITH_KNOTS ( 'NONE', 3,
 ( #2355, #87584, #18066, #10449 ),
 .UNSPECIFIED., .F., .F.,
 ( 4, 4 ),
 ( 0.000000000000000000, 9.999999999998900014E-05 ),
 .UNSPECIFIED. ) ;
#41136=CARTESIAN_POINT ( 'NONE',  ( -117.5228709571500758, -23.48783264082477729, -1.443836473390083697 ) ) ;
#41137=CARTESIAN_POINT ( 'NONE',  ( -20.89022842043660688, 4.291957016416017900, -1.500000000000002220 ) ) ;
#41138=CARTESIAN_POINT ( 'NONE',  ( -70.27422298781921484, -25.31465149953924865, 4.851635142449610250 ) ) ;
#41139=PLANE ( 'NONE',  #36764 ) ;
#41140=EDGE_CURVE ( 'NONE', #80103, #1680, #89204, .T. ) ;
#41141=CARTESIAN_POINT ( 'NONE',  ( -85.62287095715004170, -29.50248789122583659, 2.256150453626215580 ) ) ;
#41142=CARTESIAN_POINT ( 'NONE',  ( -80.60605223983722567, -25.12374756684099353, 7.097317179231969142 ) ) ;
#41143=CARTESIAN_POINT ( 'NONE',  ( -13.16310354753345990, -18.33534949228788236, -1.500000000000002220 ) ) ;
#41144=CARTESIAN_POINT ( 'NONE',  ( -40.94687764114259920, -25.04307374350000259, 7.563175304812659761 ) ) ;
#41146=FACE_OUTER_BOUND ( 'NONE', #83174, .T. ) ;
#41148=CARTESIAN_POINT ( 'NONE',  ( -19.67010641940559168, 0.002901314006966619011, 11.49999999999999645 ) ) ;
#41151=VERTEX_POINT ( 'NONE', #2982 ) ;
#41152=CARTESIAN_POINT ( 'NONE',  ( -99.52218633031425554, -23.48783264082478439, -1.443836473390063047 ) ) ;
#41154=CARTESIAN_POINT ( 'NONE',  ( -124.5899953110402549, -24.15620529776629510, 10.23563542870659404 ) ) ;
#41155=CARTESIAN_POINT ( 'NONE',  ( -88.55620429048339304, -23.47593901973091235, -1.443836447539002865 ) ) ;
#41157=CARTESIAN_POINT ( 'NONE',  ( -64.62287095715005592, -29.50248528299804818, 1.056150453629034924 ) ) ;
#41158=CARTESIAN_POINT ( 'NONE',  ( -9.637476322613308000, -17.25261889746210997, 11.49999999999998934 ) ) ;
#41159=ORIENTED_EDGE ( 'NONE', *, *, #35756, .T. ) ;
#41160=CARTESIAN_POINT ( 'NONE',  ( 12.02422309597069017, 16.21794576832014556, 11.49999999999999645 ) ) ;
#41161=CARTESIAN_POINT ( 'NONE',  ( -112.6228709571501128, -23.96177878511308634, 10.65340807706329684 ) ) ;
#41165=CARTESIAN_POINT ( 'NONE',  ( -100.3784397666924804, -25.26638541110039426, 7.561116734059481814 ) ) ;
#41166=DIRECTION ( 'NONE',  ( -3.773278334453079618E-23, 0.9999999999976377785, 2.173523156925979975E-06 ) ) ;
#41168=CARTESIAN_POINT ( 'NONE',  ( -33.58953762381672448, -23.48783264082477373, -1.443836473390074371 ) ) ;
#41169=CARTESIAN_POINT ( 'NONE',  ( -17.62595516807937557, -9.487554784798948759, -1.500000000000002220 ) ) ;
#41171=CARTESIAN_POINT ( 'NONE',  ( -58.62287095715002039, -23.94994826722515668, -0.6494450866351725304 ) ) ;
#41172=EDGE_LOOP ( 'NONE', ( #57851, #80506, #91230, #25000 ) ) ;
#41173=B_SPLINE_CURVE_WITH_KNOTS ( 'NONE', 3,
 ( #74481, #35920, #59774, #43543, #20685, #45046 ),
 .UNSPECIFIED., .F., .F.,
 ( 4, 2, 4 ),
 ( 0.000000000000000000, 0.001380764517853250335, 0.002761529035706500670 ),
 .UNSPECIFIED. ) ;
#41175=CARTESIAN_POINT ( 'NONE',  ( -52.62287095715005592, -29.50248528299804818, 1.056150453629033370 ) ) ;
#41176=CARTESIAN_POINT ( 'NONE',  ( -63.52287095715006160, -24.64965694238575011, 8.947790433994201820 ) ) ;
#41177=CARTESIAN_POINT ( 'NONE',  ( -124.6228709571500417, -24.65952944569304606, 1.056160979905705011 ) ) ;
#41178=CARTESIAN_POINT ( 'NONE',  ( -73.49610432738134591, -24.65952944569304606, 1.056160979905700126 ) ) ;
#41179=CARTESIAN_POINT ( 'NONE',  ( -45.62287095715004881, -23.47596703998600276, 11.44779298504227505 ) ) ;
#41181=CARTESIAN_POINT ( 'NONE',  ( -100.9369564999036157, -25.31392319263090229, 5.203681702801227438 ) ) ;
#41184=CARTESIAN_POINT ( 'NONE',  ( 9.670762957215185196, 17.83519281925787325, 11.49999999999998934 ) ) ;
#41185=VERTEX_POINT ( 'NONE', #96314 ) ;
#41189=CARTESIAN_POINT ( 'NONE',  ( -127.5219658841072174, -23.73791477778912551, 11.05961554403169167 ) ) ;
#41190=CARTESIAN_POINT ( 'NONE',  ( -105.6228709571501128, -24.52232992886363760, 0.6492154411906164713 ) ) ;
#41191=EDGE_CURVE ( 'NONE', #88647, #34088, #45033, .T. ) ;
#41193=AXIS2_PLACEMENT_3D ( 'NONE', #68648, #84857, #15337 ) ;
#41195=EDGE_CURVE ( 'NONE', #77364, #24634, #60475, .T. ) ;
#41196=CARTESIAN_POINT ( 'NONE',  ( -13.65698368949537311, 16.12507722524849996, 11.49999999999999645 ) ) ;
#41197=CARTESIAN_POINT ( 'NONE',  ( 8.970247382295582383, 20.24485829007567617, -1.500000000000002220 ) ) ;
#41199=CARTESIAN_POINT ( 'NONE',  ( -9.016818060619870678, -18.48156098877705844, -1.500000000000002220 ) ) ;
#41200=ORIENTED_EDGE ( 'NONE', *, *, #3031, .T. ) ;
#41201=FACE_OUTER_BOUND ( 'NONE', #35337, .T. ) ;
#41204=DIRECTION ( 'NONE',  ( 1.000000000000000000, 3.773278334444166432E-23, 8.201307841325785021E-29 ) ) ;
#41205=ORIENTED_EDGE ( 'NONE', *, *, #49916, .T. ) ;
#41206=B_SPLINE_CURVE_WITH_KNOTS ( 'NONE', 3,
 ( #86131, #78503, #9507, #16607 ),
 .UNSPECIFIED., .F., .F.,
 ( 4, 4 ),
 ( 0.000000000000000000, 9.999999999998897304E-05 ),
 .UNSPECIFIED. ) ;
#41209=CARTESIAN_POINT ( 'NONE',  ( -111.5947439173848466, -25.23257392120766340, 3.581186434512583450 ) ) ;
#41212=CARTESIAN_POINT ( 'NONE',  ( -0.2510023010970363067, -20.70922355669356563, -1.500000000000002220 ) ) ;
#41213=B_SPLINE_CURVE_WITH_KNOTS ( 'NONE', 3,
 ( #20644, #59732, #48751, #82549, #72582, #36380, #52112, #42144, #98766, #29260, #80184, #96408, #13527, #90663, #2569, #13029, #74924, #87289, #56868, #80682, #73084, #49258 ),
 .UNSPECIFIED., .F., .F.,
 ( 4, 2, 2, 2, 2, 2, 2, 2, 2, 2, 4 ),
 ( 2.168404344971008627E-19, 0.0002785781587267594124, 0.0005571563174535186080, 0.001114312634907036999, 0.001392890793633791858, 0.001671468952360546717, 0.002228625269814061421, 0.002785781587267576343, 0.003342937904721091265, 0.003900094222174607054, 0.004457250539628123710 ),
 .UNSPECIFIED. ) ;
#41214=CARTESIAN_POINT ( 'NONE',  ( -5.395268184683536639, 21.00466093859614958, 11.49999999999999645 ) ) ;
#41216=CARTESIAN_POINT ( 'NONE',  ( -60.52287095715002607, -24.63345952396938898, 9.038047939281669940 ) ) ;
#41218=CARTESIAN_POINT ( 'NONE',  ( 14.42577177192597482, -17.14957960503723911, 11.49999999999998934 ) ) ;
#41223=CARTESIAN_POINT ( 'NONE',  ( -35.50851531642891956, -23.85049219812685095, 10.88485053497527488 ) ) ;
#41225=VERTEX_POINT ( 'NONE', #44525 ) ;
#41226=CARTESIAN_POINT ( 'NONE',  ( -67.52209873245003280, -23.48786465467241058, 11.44779295918254824 ) ) ;
#41227=ORIENTED_EDGE ( 'NONE', *, *, #74619, .F. ) ;
#41228=CARTESIAN_POINT ( 'NONE',  ( -80.52287095715006160, -29.50250243563736774, 8.947779886222141599 ) ) ;
#41229=CARTESIAN_POINT ( 'NONE',  ( 7.950249384483326409, 19.69624408967213469, -1.500000000000002220 ) ) ;
#41230=ORIENTED_EDGE ( 'NONE', *, *, #20946, .T. ) ;
#41231=CARTESIAN_POINT ( 'NONE',  ( -68.62287095715008434, -23.96127896941632329, -0.6493128931037843721 ) ) ;
#41232=CARTESIAN_POINT ( 'NONE',  ( -18.37375256118794553, 11.78967355450649457, -1.500000000000002220 ) ) ;
#41233=CARTESIAN_POINT ( 'NONE',  ( -103.5888923157342276, -24.35071581493543391, 9.817618358456027039 ) ) ;
#41234=FACE_OUTER_BOUND ( 'NONE', #13225, .T. ) ;
#41235=CARTESIAN_POINT ( 'NONE',  ( -128.6228709571500417, -29.50248528299804818, 1.056150453629047137 ) ) ;
#41236=CARTESIAN_POINT ( 'NONE',  ( -4.983756199382824548, -21.29032736245130053, -1.500000000000002220 ) ) ;
#41238=ORIENTED_EDGE ( 'NONE', *, *, #93985, .T. ) ;
#41240=CARTESIAN_POINT ( 'NONE',  ( -48.89385731722059347, -25.12782558666062371, 6.392749237613702284 ) ) ;
#41241=VERTEX_POINT ( 'NONE', #14053 ) ;
#41244=ORIENTED_EDGE ( 'NONE', *, *, #73444, .F. ) ;
#41245=CARTESIAN_POINT ( 'NONE',  ( -46.62287095715004881, -29.50248528299804818, 1.056150453629033370 ) ) ;
#41246=CARTESIAN_POINT ( 'NONE',  ( -113.6228709571500559, -23.73907113216990794, -1.053371485793225260 ) ) ;
#41247=CARTESIAN_POINT ( 'NONE',  ( 10.86157628581156764, 18.25448884030880592, 11.49999999999998934 ) ) ;
#41248=CARTESIAN_POINT ( 'NONE',  ( -71.20541289166536103, -29.50249360700573931, 4.885880847770192048 ) ) ;
#41249=CARTESIAN_POINT ( 'NONE',  ( -40.85509569547110686, -25.19765059099818671, 6.732792336238610176 ) ) ;
#41250=ADVANCED_FACE ( 'NONE', ( #29290 ), #68856, .F. ) ;
#41251=VECTOR ( 'NONE', #73610, 1000.000000000000114 ) ;
#41252=DIRECTION ( 'NONE',  ( -0.000000000000000000, 2.173523156925979552E-06, -0.9999999999976378895 ) ) ;
#41253=LINE ( 'NONE', #17912, #32980 ) ;
#41254=CARTESIAN_POINT ( 'NONE',  ( -18.22486019313910077, 6.713856318530649681, -1.500000000000002220 ) ) ;
#41255=EDGE_CURVE ( 'NONE', #73282, #32756, #51136, .T. ) ;
#41256=CARTESIAN_POINT ( 'NONE',  ( -45.62923331240457969, -24.83618233451450408, 1.606449574219532384 ) ) ;
#41257=VERTEX_POINT ( 'NONE', #91184 ) ;
#41258=CARTESIAN_POINT ( 'NONE',  ( 5.544562197198338538, -18.70016399976332977, 11.49999999999999645 ) ) ;
#41260=CARTESIAN_POINT ( 'NONE',  ( -80.41358636250679126, -25.12334935364737376, 7.099569252745908443 ) ) ;
#41262=VECTOR ( 'NONE', #95354, 1000.000000000000114 ) ;
#41264=CARTESIAN_POINT ( 'NONE',  ( -75.62287095715007013, -24.92579138211019796, 1.929029949965668234 ) ) ;
#41265=FACE_OUTER_BOUND ( 'NONE', #32692, .T. ) ;
#41266=CARTESIAN_POINT ( 'NONE',  ( -80.55728237399675606, -25.24813991124032952, 7.562285528293593906 ) ) ;
#41267=CARTESIAN_POINT ( 'NONE',  ( 18.24227566675094181, -7.298356753547692755, 11.49999999999998934 ) ) ;
#41268=ORIENTED_EDGE ( 'NONE', *, *, #37654, .T. ) ;
#41269=CARTESIAN_POINT ( 'NONE',  ( -97.52287095715006160, -29.50250786944525672, 11.44777988621623166 ) ) ;
#41270=CARTESIAN_POINT ( 'NONE',  ( -59.52287095715006160, -23.48783264082477018, -1.443836473390095021 ) ) ;
#41274=CARTESIAN_POINT ( 'NONE',  ( -115.6228709571499991, -24.83620972994592435, 8.398175272781360334 ) ) ;
#41275=CARTESIAN_POINT ( 'NONE',  ( -97.55489214582006241, -23.96169478059713853, 10.65365249895717703 ) ) ;
#41276=CARTESIAN_POINT ( 'NONE',  ( -94.62287095715005592, -23.48783264082478794, -1.443836473390063491 ) ) ;
#41278=FACE_OUTER_BOUND ( 'NONE', #65365, .T. ) ;
#41280=CARTESIAN_POINT ( 'NONE',  ( -7.573260116017839216, 18.43532004384545786, -1.500000000000002220 ) ) ;
#41281=CARTESIAN_POINT ( 'NONE',  ( -75.55895386407497938, -23.85049219812685806, 10.88485053497527488 ) ) ;
#41282=CARTESIAN_POINT ( 'NONE',  ( -13.56193660873917395, -14.51407242162769151, -1.500000000000002220 ) ) ;
#41284=DIRECTION ( 'NONE',  ( 0.000000000000000000, -0.9999999999976377785, -2.173523156925979128E-06 ) ) ;
#41287=AXIS2_PLACEMENT_3D ( 'NONE', #91045, #29646, #36768 ) ;
#41289=CARTESIAN_POINT ( 'NONE',  ( 19.40640353424967302, -7.489167304209242815, 11.49999999999999645 ) ) ;
#41290=FACE_OUTER_BOUND ( 'NONE', #22232, .T. ) ;
#41292=CARTESIAN_POINT ( 'NONE',  ( 22.50852769316577096, -3.342225187595919689, 11.49999999999999645 ) ) ;
#41293=ORIENTED_EDGE ( 'NONE', *, *, #90786, .F. ) ;
#41297=ADVANCED_FACE ( 'NONE', ( #37905 ), #75952, .T. ) ;
#41298=B_SPLINE_CURVE_WITH_KNOTS ( 'NONE', 3,
 ( #66901, #97331, #27819, #42566 ),
 .UNSPECIFIED., .F., .F.,
 ( 4, 4 ),
 ( 2.775557561562891351E-17, 0.0001000000000000167286 ),
 .UNSPECIFIED. ) ;
#41299=CARTESIAN_POINT ( 'NONE',  ( -18.67835518149133378, -7.740158416121700746, -1.500000000000002220 ) ) ;
#41300=DIRECTION ( 'NONE',  ( 3.773278334444166432E-23, -1.000000000000000000, 0.000000000000000000 ) ) ;
#41301=CARTESIAN_POINT ( 'NONE',  ( -40.67156841055674477, -25.30545518805434568, 5.059772659950606766 ) ) ;
#41302=EDGE_CURVE ( 'NONE', #23301, #1643, #91891, .T. ) ;
#41303=CARTESIAN_POINT ( 'NONE',  ( -100.6228709571500559, -24.83602698348162008, 1.605859176311265735 ) ) ;
#41306=PLANE ( 'NONE',  #58251 ) ;
#41308=CARTESIAN_POINT ( 'NONE',  ( -4.560224734120114753, 19.45435480350565882, -1.500000000000002220 ) ) ;
#41309=EDGE_CURVE ( 'NONE', #99816, #28831, #84072, .T. ) ;
#41310=CARTESIAN_POINT ( 'NONE',  ( -8.674659061502078217, -19.08593140856894621, 11.49999999999999645 ) ) ;
#41311=CARTESIAN_POINT ( 'NONE',  ( -27.89254357189496858, -24.66661246132309415, 8.246170428369305583 ) ) ;
#41313=CARTESIAN_POINT ( 'NONE',  ( 18.76863814860013235, 11.56883167669432133, -1.500000000000002220 ) ) ;
#41314=EDGE_CURVE ( 'NONE', #6893, #70136, #82577, .T. ) ;
#41315=AXIS2_PLACEMENT_3D ( 'NONE', #50788, #83216, #28937 ) ;
#41317=ORIENTED_EDGE ( 'NONE', *, *, #89217, .T. ) ;
#41318=CARTESIAN_POINT ( 'NONE',  ( -47.62287095715004170, -24.65952944569304250, 1.056160979905693686 ) ) ;
#41320=DIRECTION ( 'NONE',  ( -3.773278334444166432E-23, 1.000000000000000000, 0.000000000000000000 ) ) ;
#41322=CARTESIAN_POINT ( 'NONE',  ( -123.6228709571500275, -23.95044443724991012, 10.65354141964650125 ) ) ;
#41326=DIRECTION ( 'NONE',  ( 3.773278334444167608E-23, -1.000000000000000000, 0.000000000000000000 ) ) ;
#41327=CARTESIAN_POINT ( 'NONE',  ( -94.62287095715009855, -24.33927499327855415, 9.819080762295811837 ) ) ;
#41328=EDGE_CURVE ( 'NONE', #21186, #42265, #82086, .T. ) ;
#41329=CARTESIAN_POINT ( 'NONE',  ( 20.13950599927006735, 4.067174238878714654, -1.500000000000002220 ) ) ;
#41332=PLANE ( 'NONE',  #8874 ) ;
#41335=CARTESIAN_POINT ( 'NONE',  ( -18.48265707593502327, -12.51853143457666562, -1.500000000000002220 ) ) ;
#41336=AXIS2_PLACEMENT_3D ( 'NONE', #78360, #56055, #23068 ) ;
#41337=CARTESIAN_POINT ( 'NONE',  ( -81.62287095715005592, -23.47593901973091235, -1.443836447539004642 ) ) ;
#41338=CARTESIAN_POINT ( 'NONE',  ( -31.52287095715004739, -23.48783264083373723, -1.443836473376154617 ) ) ;
#41339=ORIENTED_EDGE ( 'NONE', *, *, #19892, .T. ) ;
#41340=CARTESIAN_POINT ( 'NONE',  ( -32.62287095715007013, -23.95044443724992078, 10.65354141964649592 ) ) ;
#41341=CARTESIAN_POINT ( 'NONE',  ( -73.52287095715010423, -24.51283580621364067, 0.6167428607019833642 ) ) ;
#41342=CARTESIAN_POINT ( 'NONE',  ( 20.84756458399398937, 0.1950554047328266483, -1.500000000000002220 ) ) ;
#41344=CARTESIAN_POINT ( 'NONE',  ( -51.55620429048339304, -24.64898659630528499, 1.056161002820822814 ) ) ;
#41345=ORIENTED_EDGE ( 'NONE', *, *, #15433, .F. ) ;
#41346=ORIENTED_EDGE ( 'NONE', *, *, #34769, .F. ) ;
#41347=CARTESIAN_POINT ( 'NONE',  ( -69.79804103094413392, -25.25935328972423832, 7.463048828822199887 ) ) ;
#41348=CARTESIAN_POINT ( 'NONE',  ( -11.20027426441765961, 17.80179601997297212, -1.500000000000002220 ) ) ;
#41349=EDGE_LOOP ( 'NONE', ( #62444, #79770, #41114, #82813 ) ) ;
#41352=CARTESIAN_POINT ( 'NONE',  ( -120.6249267159150378, -24.63419186844610920, 9.035850630976920428 ) ) ;
#41353=CARTESIAN_POINT ( 'NONE',  ( -86.63220028990764376, -24.15620529776628445, 10.23563542870660292 ) ) ;
#41354=CARTESIAN_POINT ( 'NONE',  ( -73.52287095715007581, -24.65952944569304606, 1.056160979905697239 ) ) ;
#41355=CARTESIAN_POINT ( 'NONE',  ( 21.69746526873944958, -0.4026533170205861545, -1.500000000000002220 ) ) ;
#41357=CARTESIAN_POINT ( 'NONE',  ( -21.14947813473477822, 6.846651710974520633, 11.49999999999999645 ) ) ;
#41358=EDGE_LOOP ( 'NONE', ( #99476, #49954, #9362, #33970 ) ) ;
#41359=B_SPLINE_CURVE_WITH_KNOTS ( 'NONE', 3,
 ( #21193, #29313, #61286, #21686, #90222, #20696, #75976, #29812 ),
 .UNSPECIFIED., .F., .F.,
 ( 4, 2, 2, 4 ),
 ( 6.384118678617175936E-06, 0.002007151183507260156, 0.003007534715921581642, 0.004007918248335903127 ),
 .UNSPECIFIED. ) ;
#41360=CARTESIAN_POINT ( 'NONE',  ( -50.82761139903328029, -25.31441737940271253, 5.269904038178990113 ) ) ;
#41362=CARTESIAN_POINT ( 'NONE',  ( -54.58953762381672448, -24.64898659630528854, 1.056161002820823258 ) ) ;
#41363=ORIENTED_EDGE ( 'NONE', *, *, #45875, .T. ) ;
#41364=B_SPLINE_CURVE_WITH_KNOTS ( 'NONE', 3,
 ( #78257, #9258, #56462, #71676 ),
 .UNSPECIFIED., .F., .F.,
 ( 4, 4 ),
 ( 0.2006432744510161237, 0.2096497057231316852 ),
 .UNSPECIFIED. ) ;
#41366=EDGE_LOOP ( 'NONE', ( #30732, #78513, #64081, #2534 ) ) ;
#41368=VERTEX_POINT ( 'NONE', #63258 ) ;
#41369=B_SPLINE_CURVE_WITH_KNOTS ( 'NONE', 3,
 ( #40637, #25902, #16282, #33020 ),
 .UNSPECIFIED., .F., .F.,
 ( 4, 4 ),
 ( 0.9812006513676874153, 0.9902070826398029491 ),
 .UNSPECIFIED. ) ;
#41370=AXIS2_PLACEMENT_3D ( 'NONE', #16815, #47779, #40160 ) ;
#41372=ADVANCED_FACE ( 'NONE', ( #32788 ), #70355, .F. ) ;
#41373=CARTESIAN_POINT ( 'NONE',  ( -1.972954090310384379, -20.06304030521763337, -1.500000000000002220 ) ) ;
#41374=CARTESIAN_POINT ( 'NONE',  ( -66.52287095715007581, -24.50321055353804311, 9.387540953477518713 ) ) ;
#41377=CARTESIAN_POINT ( 'NONE',  ( -130.5728709571500588, -23.92955623466736270, -0.8917680458859206238 ) ) ;
#41378=CARTESIAN_POINT ( 'NONE',  ( -20.95026660567425481, -7.857139728745305973, -1.500000000000002220 ) ) ;
#41380=ORIENTED_EDGE ( 'NONE', *, *, #20535, .F. ) ;
#41381=CARTESIAN_POINT ( 'NONE',  ( -112.5934603124331517, -23.73791477778912551, 11.05961554403169878 ) ) ;
#41382=CARTESIAN_POINT ( 'NONE',  ( -44.62287095715004881, -23.47593901973091235, -1.443836447539011525 ) ) ;
#41383=CARTESIAN_POINT ( 'NONE',  ( -39.82981181716615282, -25.31535245520623079, 4.920765160820281814 ) ) ;
#41385=CARTESIAN_POINT ( 'NONE',  ( -30.59161074801509272, -24.82959736273286566, 8.370978854367633559 ) ) ;
#41386=CARTESIAN_POINT ( 'NONE',  ( -2.459534284235005863, 19.42625828800391119, -1.500000000000002220 ) ) ;
#41388=ORIENTED_EDGE ( 'NONE', *, *, #62216, .T. ) ;
#41389=CARTESIAN_POINT ( 'NONE',  ( -10.32266838563235467, 18.89866041204108527, 11.49999999999998934 ) ) ;
#41391=CARTESIAN_POINT ( 'NONE',  ( -80.46709582760330193, -25.31572646173322383, 4.967766229843499026 ) ) ;
#41392=CARTESIAN_POINT ( 'NONE',  ( -53.58953762381671737, -23.47596703998600276, 11.44779298504227505 ) ) ;
#41394=CARTESIAN_POINT ( 'NONE',  ( -13.60431050971674694, 18.46711184989817411, -1.500000000000002220 ) ) ;
#41395=VECTOR ( 'NONE', #49190, 1000.000000000000114 ) ;
#41398=CARTESIAN_POINT ( 'NONE',  ( -70.52287095715007581, -29.50250786944525672, 11.44777988621623699 ) ) ;
#41399=DIRECTION ( 'NONE',  ( 0.000000000000000000, -0.9999999999976377785, -2.173523156925979975E-06 ) ) ;
#41400=CARTESIAN_POINT ( 'NONE',  ( -9.210493908506615313, -17.87979239004878451, 11.49999999999999645 ) ) ;
#41402=CARTESIAN_POINT ( 'NONE',  ( -32.48906222994808246, -24.35071581493542681, 9.817618358456035921 ) ) ;
#41403=CARTESIAN_POINT ( 'NONE',  ( -111.6228709571500559, -29.50250243563736774, 8.947779886222136270 ) ) ;
#41405=CARTESIAN_POINT ( 'NONE',  ( -82.52287095715003318, -24.50321055353804311, 9.387540953477522265 ) ) ;
#41406=CARTESIAN_POINT ( 'NONE',  ( 19.67252036444665109, 2.607452956813616218, 11.49999999999998934 ) ) ;
#41409=CARTESIAN_POINT ( 'NONE',  ( -18.83419513347712737, -5.836681878196540829, -1.500000000000002220 ) ) ;
#41410=VECTOR ( 'NONE', #11826, 1000.000000000000114 ) ;
#41412=CARTESIAN_POINT ( 'NONE',  ( -101.3738023147422638, -25.26303730729093999, 3.986250639247583827 ) ) ;
#41414=CARTESIAN_POINT ( 'NONE',  ( -57.52287095715004739, -24.33927499327854349, 9.819080762295813614 ) ) ;
#41415=CARTESIAN_POINT ( 'NONE',  ( -39.42660405732974738, -25.30265167098723822, 5.336464896208934938 ) ) ;
#41416=CARTESIAN_POINT ( 'NONE',  ( -4.647353109605855792, 20.10343637636090719, 11.49999999999999645 ) ) ;
#41419=CARTESIAN_POINT ( 'NONE',  ( 16.66146196086182130, -15.28366505690825328, 11.49999999999999645 ) ) ;
#41421=CARTESIAN_POINT ( 'NONE',  ( -53.58953762381671737, -24.65952944569304250, 1.056160979905693686 ) ) ;
#41422=CARTESIAN_POINT ( 'NONE',  ( -51.25929116468429925, -25.28952511681641013, 4.204884817874903646 ) ) ;
#41423=CARTESIAN_POINT ( 'NONE',  ( -27.68651082257922980, -24.78174777341091328, 2.274903344755643708 ) ) ;
#41424=EDGE_CURVE ( 'NONE', #60391, #11305, #7443, .T. ) ;
#41425=LINE ( 'NONE', #97202, #69493 ) ;
#41426=DIRECTION ( 'NONE',  ( -3.773278334453079030E-23, 0.9999999999976377785, 2.173523156925979128E-06 ) ) ;
#41428=CARTESIAN_POINT ( 'NONE',  ( 6.977686149863070675, -22.03694335537135984, 11.49999999999999645 ) ) ;
#41429=CARTESIAN_POINT ( 'NONE',  ( -21.78311099772515647, -6.823855485095160489, -1.500000000000002220 ) ) ;
#41430=CARTESIAN_POINT ( 'NONE',  ( -111.3346403563335514, -25.26931265113162794, 4.061649485443762586 ) ) ;
#41431=CARTESIAN_POINT ( 'NONE',  ( -79.52287095715004739, -23.48783264082476663, -1.443836473390090358 ) ) ;
#41432=CARTESIAN_POINT ( 'NONE',  ( -63.65418217327448502, -23.48786465467241413, 11.44779295918254824 ) ) ;
#41433=VECTOR ( 'NONE', #45167, 1000.000000000000114 ) ;
#41434=EDGE_CURVE ( 'NONE', #30205, #85507, #60279, .T. ) ;
#41435=CARTESIAN_POINT ( 'NONE',  ( 17.87336509531889561, -13.68139028912531785, 11.49999999999999645 ) ) ;
#41436=ORIENTED_EDGE ( 'NONE', *, *, #78773, .F. ) ;
#41437=CARTESIAN_POINT ( 'NONE',  ( -36.62287095715004170, -23.47596703998600276, 11.44779298504227505 ) ) ;
#41438=CARTESIAN_POINT ( 'NONE',  ( -21.51515180086577317, 4.489188270810763548, 11.49999999999998934 ) ) ;
#41440=DIRECTION ( 'NONE',  ( -3.773278334453079618E-23, 0.9999999999976377785, 2.173523156925979975E-06 ) ) ;
#41441=FACE_OUTER_BOUND ( 'NONE', #87014, .T. ) ;
#41442=CARTESIAN_POINT ( 'NONE',  ( -66.62287095715005592, -29.50247984919015209, -1.443849546365055359 ) ) ;
#41444=DIRECTION ( 'NONE',  ( 0.000000000000000000, 0.9999999999976377785, 2.173523156925979128E-06 ) ) ;
#41447=CARTESIAN_POINT ( 'NONE',  ( -69.52287095715006160, -23.47596703998600631, 11.44779298504228748 ) ) ;
#41448=CARTESIAN_POINT ( 'NONE',  ( 12.01435098137705637, -16.61664908515649941, -1.500000000000002220 ) ) ;
#41449=ORIENTED_EDGE ( 'NONE', *, *, #24368, .F. ) ;
#41451=VERTEX_POINT ( 'NONE', #78952 ) ;
#41452=ORIENTED_EDGE ( 'NONE', *, *, #65724, .T. ) ;
#41453=CARTESIAN_POINT ( 'NONE',  ( -72.22287095715007865, -23.47593901973090169, -1.443836447538997536 ) ) ;
#41454=CARTESIAN_POINT ( 'NONE',  ( 20.31487730549432413, -11.01532776123576518, 11.49999999999998934 ) ) ;
#41455=CARTESIAN_POINT ( 'NONE',  ( -104.6266608578756063, -24.35071581493543746, 9.817618358456019934 ) ) ;
#41456=ADVANCED_FACE ( 'NONE', ( #1850 ), #92677, .T. ) ;
#41457=CARTESIAN_POINT ( 'NONE',  ( -0.6891947355827284794, 20.32259304938107292, -1.500000000000002220 ) ) ;
#41458=ORIENTED_EDGE ( 'NONE', *, *, #19191, .T. ) ;
#41459=DIRECTION ( 'NONE',  ( -0.000000000000000000, 2.173523156925979552E-06, -0.9999999999976378895 ) ) ;
#41460=DIRECTION ( 'NONE',  ( -3.773278334453079030E-23, 0.9999999999976377785, 2.173523156925979128E-06 ) ) ;
#41461=CARTESIAN_POINT ( 'NONE',  ( -114.6228709571500559, -29.50248528299804818, 1.056150453629043584 ) ) ;
#41462=CARTESIAN_POINT ( 'NONE',  ( -70.48847287023792774, -24.92564183028979130, 1.928384488918253536 ) ) ;
#41464=LINE ( 'NONE', #10503, #98644 ) ;
#41465=CARTESIAN_POINT ( 'NONE',  ( -120.6228709571500417, -29.50249982740957577, 7.747779886224967605 ) ) ;
#41467=CARTESIAN_POINT ( 'NONE',  ( 4.358738815032396907, -20.29635662749097236, -1.500000000000002220 ) ) ;
#41469=DIRECTION ( 'NONE',  ( 3.773278334444166432E-23, -1.000000000000000000, 0.000000000000000000 ) ) ;
#41472=CARTESIAN_POINT ( 'NONE',  ( -82.58953762381672448, -24.64898659630367916, 1.056161002820385830 ) ) ;
#41473=CARTESIAN_POINT ( 'NONE',  ( -107.6228709571500701, -24.64898659630368272, 1.056161002820831474 ) ) ;
#41474=ORIENTED_EDGE ( 'NONE', *, *, #73444, .T. ) ;
#41478=CARTESIAN_POINT ( 'NONE',  ( -123.5562042904833930, -24.64965694238575011, 8.947790433994185832 ) ) ;
#41479=AXIS2_PLACEMENT_3D ( 'NONE', #63750, #70336, #24151 ) ;
#41480=B_SPLINE_CURVE_WITH_KNOTS ( 'NONE', 3,
 ( #18355, #34089, #49322, #29343 ),
 .UNSPECIFIED., .F., .F.,
 ( 4, 4 ),
 ( 0.6092082805810596913, 0.6102090276218251619 ),
 .UNSPECIFIED. ) ;
#41481=CARTESIAN_POINT ( 'NONE',  ( -34.52287095715006160, -23.48786465467240347, 11.44779295918255357 ) ) ;
#41483=CARTESIAN_POINT ( 'NONE',  ( 4.500060333422437608, -21.59917750860068963, 11.49999999999999645 ) ) ;
#41484=ORIENTED_EDGE ( 'NONE', *, *, #56792, .T. ) ;
#41486=CARTESIAN_POINT ( 'NONE',  ( -103.5979499207285954, -23.48783264082477018, -1.443836473390091246 ) ) ;
#41487=CARTESIAN_POINT ( 'NONE',  ( -20.50338545487000275, 9.463669735852004550, -1.500000000000002220 ) ) ;
#41489=DIRECTION ( 'NONE',  ( -3.773278334453080206E-23, 0.9999999999976377785, 2.173523156925979975E-06 ) ) ;
#41490=ORIENTED_EDGE ( 'NONE', *, *, #93348, .T. ) ;
#41491=EDGE_LOOP ( 'NONE', ( #34860, #48965, #43493, #71327, #21926, #97487, #30731, #65925 ) ) ;
#41492=CARTESIAN_POINT ( 'NONE',  ( -59.52287095715004739, -24.66019654487199375, 8.947790411086128159 ) ) ;
#41493=EDGE_CURVE ( 'NONE', #86903, #25620, #66407, .T. ) ;
#41495=VERTEX_POINT ( 'NONE', #47525 ) ;
#41496=CARTESIAN_POINT ( 'NONE',  ( -19.86647519178106691, -7.318714840676754818, -1.500000000000002220 ) ) ;
#41497=DIRECTION ( 'NONE',  ( -3.773278334444166432E-23, 1.000000000000000000, 0.000000000000000000 ) ) ;
#41498=CARTESIAN_POINT ( 'NONE',  ( -78.94303308397306296, -25.27791628310042427, 5.977536664604797600 ) ) ;
#41501=CARTESIAN_POINT ( 'NONE',  ( 1.019757120859956512, 22.21710203930399175, -1.500000000000002220 ) ) ;
#41502=CARTESIAN_POINT ( 'NONE',  ( -74.62287095715005592, -24.64965695001467694, 8.947790433994184056 ) ) ;
#41505=LINE ( 'NONE', #81061, #78328 ) ;
#41506=CARTESIAN_POINT ( 'NONE',  ( -14.46832242630667942, -12.86894606327920876, 11.49999999999999645 ) ) ;
#41509=CARTESIAN_POINT ( 'NONE',  ( -17.65537929698502495, 8.214918384300796461, 11.49999999999998934 ) ) ;
#41510=CARTESIAN_POINT ( 'NONE',  ( -15.65470850568805083, 14.63654280257262386, 11.49999999999998934 ) ) ;
#41511=CARTESIAN_POINT ( 'NONE',  ( -56.62287095715009144, -23.94994826722566117, -0.6494450866342736939 ) ) ;
#41512=CARTESIAN_POINT ( 'NONE',  ( -26.59970390766585169, -24.92774742939907284, 1.981116289752363757 ) ) ;
#41513=CARTESIAN_POINT ( 'NONE',  ( -32.62287095715004881, -29.50250786944525672, 11.44777988621624409 ) ) ;
#41514=CARTESIAN_POINT ( 'NONE',  ( -120.6228709571500559, -23.48786465467241769, 11.44779295918253759 ) ) ;
#41515=B_SPLINE_CURVE_WITH_KNOTS ( 'NONE', 3,
 ( #59596, #83407, #81923, #89538, #89043, #11911, #82906, #90038 ),
 .UNSPECIFIED., .F., .F.,
 ( 4, 2, 2, 4 ),
 ( 6.384118678617664674E-06, 0.002007151183507262758, 0.003007534715921585545, 0.004007918248335907464 ),
 .UNSPECIFIED. ) ;
#41516=CARTESIAN_POINT ( 'NONE',  ( 0.9741843557120299923, -22.74547949729550922, -1.500000000000002220 ) ) ;
#41517=B_SPLINE_CURVE_WITH_KNOTS ( 'NONE', 3,
 ( #74417, #96755, #27254, #13003 ),
 .UNSPECIFIED., .F., .F.,
 ( 4, 4 ),
 ( 0.000000000000000000, 0.0001000000000000167422 ),
 .UNSPECIFIED. ) ;
#41518=EDGE_CURVE ( 'NONE', #39996, #36540, #78409, .T. ) ;
#41520=CARTESIAN_POINT ( 'NONE',  ( -106.5861024369675079, -24.66019654487200441, 8.947790411086108620 ) ) ;
#41521=CARTESIAN_POINT ( 'NONE',  ( -98.62287095715012697, -24.51283580621365132, 0.6167428607019801445 ) ) ;
#41522=CARTESIAN_POINT ( 'NONE',  ( 15.94990109002195489, -11.90149544800030590, 11.49999999999999645 ) ) ;
#41523=CARTESIAN_POINT ( 'NONE',  ( -104.5889287620974244, -24.34968618360934300, 0.1864209137778872205 ) ) ;
#41524=ADVANCED_FACE ( 'NONE', ( #86075 ), #54637, .F. ) ;
#41525=CARTESIAN_POINT ( 'NONE',  ( -39.58691133940545370, -24.35071581493543036, 9.817618358456035921 ) ) ;
#41527=ORIENTED_EDGE ( 'NONE', *, *, #82458, .T. ) ;
#41529=CARTESIAN_POINT ( 'NONE',  ( -77.52287095715010423, -23.96127896941631974, -0.6493128931038042451 ) ) ;
#41530=CARTESIAN_POINT ( 'NONE',  ( -10.61912389536305490, -18.88692380039396213, 11.49999999999998934 ) ) ;
#41532=CARTESIAN_POINT ( 'NONE',  ( -93.62287095715005592, -24.65952944569304606, 1.056160979905701236 ) ) ;
#41533=CARTESIAN_POINT ( 'NONE',  ( -14.34788840963776124, 13.16932220997287928, -1.500000000000002220 ) ) ;
#41534=EDGE_CURVE ( 'NONE', #39987, #16850, #33674, .T. ) ;
#41540=DIRECTION ( 'NONE',  ( -1.000000000000000000, -3.773278334444167608E-23, -8.201307833595939069E-29 ) ) ;
#41541=CARTESIAN_POINT ( 'NONE',  ( 7.241121213506172438, 19.11196469071355963, 11.49999999999999645 ) ) ;
#41543=VECTOR ( 'NONE', #32945, 1000.000000000000114 ) ;
#41545=ORIENTED_EDGE ( 'NONE', *, *, #71542, .T. ) ;
#41546=CARTESIAN_POINT ( 'NONE',  ( -62.62287095715004881, -24.65952944569304606, 1.056160979905693909 ) ) ;
#41548=CARTESIAN_POINT ( 'NONE',  ( -49.52287095715006160, -23.47596703998600631, 11.44779298504229104 ) ) ;
#41551=AXIS2_PLACEMENT_3D ( 'NONE', #7182, #69087, #100012 ) ;
#41552=EDGE_CURVE ( 'NONE', #27354, #40387, #31136, .T. ) ;
#41554=CARTESIAN_POINT ( 'NONE',  ( -31.79944283184904563, -24.87479601683089570, 8.247789944647550442 ) ) ;
#41555=VERTEX_POINT ( 'NONE', #48027 ) ;
#41556=CARTESIAN_POINT ( 'NONE',  ( -66.59259126670630735, -24.15620529776628089, 10.23563542870660470 ) ) ;
#41559=CARTESIAN_POINT ( 'NONE',  ( -22.04953120734539240, -6.464106996104416858, 11.49999999999999645 ) ) ;
#41560=CARTESIAN_POINT ( 'NONE',  ( 6.135622925040504327, -21.92205258971886650, -1.500000000000002220 ) ) ;
#41561=CARTESIAN_POINT ( 'NONE',  ( -110.5481088315369504, -25.00182538069147142, 7.747789668545045139 ) ) ;
#41563=CARTESIAN_POINT ( 'NONE',  ( -90.62479129791826438, -24.92564183028979130, 1.928384488918253536 ) ) ;
#41565=CARTESIAN_POINT ( 'NONE',  ( -44.52287095715004739, -23.48783264082477018, -1.443836473390094577 ) ) ;
#41566=CARTESIAN_POINT ( 'NONE',  ( -20.57654891367511851, 7.437132321665034240, 11.49999999999998934 ) ) ;
#41568=CARTESIAN_POINT ( 'NONE',  ( -70.62287095715005592, -24.99132157543083821, 2.256160258750667502 ) ) ;
#41570=CARTESIAN_POINT ( 'NONE',  ( -26.17111397533802730, -24.91964606936674187, 3.942482870127836048 ) ) ;
#41572=CARTESIAN_POINT ( 'NONE',  ( -98.99594346619821295, -25.25460612665171212, 5.589964028470313373 ) ) ;
#41574=CARTESIAN_POINT ( 'NONE',  ( -1.067026067711715154, -20.38227831319515460, 11.49999999999998934 ) ) ;
#41576=ORIENTED_EDGE ( 'NONE', *, *, #24445, .T. ) ;
#41577=CARTESIAN_POINT ( 'NONE',  ( 22.09143763772896918, 6.410036269187016522, 11.49999999999998934 ) ) ;
#41578=CARTESIAN_POINT ( 'NONE',  ( -78.62287095715005592, -24.64898659630367916, 1.056161002820826145 ) ) ;
#41580=ORIENTED_EDGE ( 'NONE', *, *, #71459, .F. ) ;
#41581=VECTOR ( 'NONE', #58310, 1000.000000000000114 ) ;
#41584=EDGE_CURVE ( 'NONE', #32620, #35375, #7076, .T. ) ;
#41587=CARTESIAN_POINT ( 'NONE',  ( -119.4728709572981842, -25.30561158020721635, 5.197944563078277014 ) ) ;
#41588=CARTESIAN_POINT ( 'NONE',  ( -6.079122355442096115, 20.50309271558274915, 11.49999999999999645 ) ) ;
#41589=VERTEX_POINT ( 'NONE', #57646 ) ;
#41591=CARTESIAN_POINT ( 'NONE',  ( -9.187330254778467875, -20.22999604658808082, 11.49999999999998934 ) ) ;
#41592=CARTESIAN_POINT ( 'NONE',  ( -19.50335911044312098, -6.847048061534898977, 11.49999999999998934 ) ) ;
#41595=DIRECTION ( 'NONE',  ( 0.000000000000000000, 0.9999999999976377785, 2.173523156925979975E-06 ) ) ;
#41596=ORIENTED_EDGE ( 'NONE', *, *, #83211, .F. ) ;
#41597=B_SPLINE_CURVE_WITH_KNOTS ( 'NONE', 3,
 ( #70343, #86062, #47512, #69338 ),
 .UNSPECIFIED., .F., .F.,
 ( 4, 4 ),
 ( 0.000000000000000000, 0.0001000000000000167422 ),
 .UNSPECIFIED. ) ;
#41598=CARTESIAN_POINT ( 'NONE',  ( -80.62287095715005592, -23.47593901973091235, -1.443836447539004642 ) ) ;
#41602=CARTESIAN_POINT ( 'NONE',  ( -14.93763623016880082, -14.57113377498261997, -1.500000000000002220 ) ) ;
#41603=CARTESIAN_POINT ( 'NONE',  ( 8.256513476402210117, 20.27555108428041208, 11.49999999999999645 ) ) ;
#41604=B_SPLINE_CURVE_WITH_KNOTS ( 'NONE', 3,
 ( #27907, #58863, #5564, #75562 ),
 .UNSPECIFIED., .F., .F.,
 ( 4, 4 ),
 ( 0.000000000000000000, 9.999999999998897304E-05 ),
 .UNSPECIFIED. ) ;
#41605=CARTESIAN_POINT ( 'NONE',  ( -26.38306202989770455, -24.77993590978327276, 6.654069811898469133 ) ) ;
#41607=CARTESIAN_POINT ( 'NONE',  ( 22.48569338394020534, -0.9006126209707296937, -1.500000000000002220 ) ) ;
#41609=CARTESIAN_POINT ( 'NONE',  ( -18.74228827200876779, -9.293929619069025705, -1.500000000000002220 ) ) ;
#41610=CARTESIAN_POINT ( 'NONE',  ( -38.48527873623334017, -24.51314013834316086, 0.6176544820404135105 ) ) ;
#41611=DIRECTION ( 'NONE',  ( -3.773278334453079618E-23, 0.9999999999976377785, 2.173523156925978705E-06 ) ) ;
#41613=EDGE_LOOP ( 'NONE', ( #29040, #87876, #72671, #98519 ) ) ;
#41614=ORIENTED_EDGE ( 'NONE', *, *, #98841, .F. ) ;
#41615=ORIENTED_EDGE ( 'NONE', *, *, #50918, .F. ) ;
#41616=FACE_OUTER_BOUND ( 'NONE', #78386, .T. ) ;
#41617=EDGE_LOOP ( 'NONE', ( #25421, #47113, #39129, #13383 ) ) ;
#41619=CARTESIAN_POINT ( 'NONE',  ( 5.397486108853063236, 20.74927772461418485, -1.500000000000002220 ) ) ;
#41620=VERTEX_POINT ( 'NONE', #49032 ) ;
#41622=AXIS2_PLACEMENT_3D ( 'NONE', #44834, #14858, #60567 ) ;
#41623=CARTESIAN_POINT ( 'NONE',  ( 11.82777538550527119, 17.46297031709455183, -1.500000000000002220 ) ) ;
#41624=CARTESIAN_POINT ( 'NONE',  ( -30.53645441241393499, -24.83558246553552706, 8.370654131274084975 ) ) ;
#41625=DIRECTION ( 'NONE',  ( 0.000000000000000000, -0.9999999999976377785, -2.173523156925979975E-06 ) ) ;
#41628=CARTESIAN_POINT ( 'NONE',  ( -101.5506399398690007, -24.34968618360934300, 0.1864209137778871928 ) ) ;
#41629=CARTESIAN_POINT ( 'NONE',  ( -109.8280019483771497, -25.31620647586430906, 5.181285762822000152 ) ) ;
#41630=CARTESIAN_POINT ( 'NONE',  ( 4.500060333422437608, -21.59917750860068963, -1.500000000000002220 ) ) ;
#41631=ORIENTED_EDGE ( 'NONE', *, *, #100039, .F. ) ;
#41632=CARTESIAN_POINT ( 'NONE',  ( -116.5939885159102261, -23.48783264082478439, -1.443836473390061936 ) ) ;
#41634=CARTESIAN_POINT ( 'NONE',  ( -41.47025245262053517, -25.27955988164092105, 5.160615522818375212 ) ) ;
#41636=CARTESIAN_POINT ( 'NONE',  ( -62.51545974119872540, -23.73791477778911840, 11.05961554403171121 ) ) ;
#41637=CARTESIAN_POINT ( 'NONE',  ( -53.62287095715005592, -29.50250786944525672, 11.44777988621624054 ) ) ;
#41639=CARTESIAN_POINT ( 'NONE',  ( -13.37813101364405100, 16.61575060780308277, 11.49999999999998934 ) ) ;
#41640=CARTESIAN_POINT ( 'NONE',  ( -29.52287095715006160, -29.50247984919040434, -1.443849432928222987 ) ) ;
#41641=CARTESIAN_POINT ( 'NONE',  ( -117.5228709571500332, -24.66019654487200441, 8.947790411086108620 ) ) ;
#41644=CARTESIAN_POINT ( 'NONE',  ( -16.68516988606489448, 15.22057433622007316, -1.500000000000002220 ) ) ;
#41645=EDGE_CURVE ( 'NONE', #58910, #99120, #65150, .T. ) ;
#41646=CARTESIAN_POINT ( 'NONE',  ( -83.62287095715007013, -24.66019654487199730, 8.947790411086126383 ) ) ;
#41648=CARTESIAN_POINT ( 'NONE',  ( -35.62287095715005592, -23.48786465467240347, 11.44779295918255180 ) ) ;
#41649=CARTESIAN_POINT ( 'NONE',  ( -122.6228709571500843, -23.94994826722515668, -0.6494450866351679785 ) ) ;
#41650=CARTESIAN_POINT ( 'NONE',  ( -19.67082186522023690, -1.387426831159568108, 11.49999999999999645 ) ) ;
#41651=DIRECTION ( 'NONE',  ( -3.773278334444167608E-23, 1.000000000000000000, 0.000000000000000000 ) ) ;
#41652=CARTESIAN_POINT ( 'NONE',  ( -73.52287095715007581, -24.64965694238407323, 8.947790433994200043 ) ) ;
#41653=EDGE_LOOP ( 'NONE', ( #94382, #2793, #34164, #77605 ) ) ;
#41654=LINE ( 'NONE', #50261, #44187 ) ;
#41656=CARTESIAN_POINT ( 'NONE',  ( -124.5909694504235148, -23.73791477778912551, 11.05961554403169878 ) ) ;
#41660=CARTESIAN_POINT ( 'NONE',  ( -91.22287095715003602, -23.47593901973090169, -1.443836447538996870 ) ) ;
#41662=ADVANCED_FACE ( 'NONE', ( #57152 ), #7885, .T. ) ;
#41663=FACE_OUTER_BOUND ( 'NONE', #16348, .T. ) ;
#41664=DIRECTION ( 'NONE',  ( 0.000000000000000000, 0.9999999999976377785, 2.173523156925979128E-06 ) ) ;
#41665=CARTESIAN_POINT ( 'NONE',  ( 13.37688099249405127, 14.58279310912311111, 11.49999999999998934 ) ) ;
#41666=B_SPLINE_CURVE_WITH_KNOTS ( 'NONE', 3,
 ( #56355, #33001, #60596, #83906 ),
 .UNSPECIFIED., .F., .F.,
 ( 4, 4 ),
 ( 1.387778780781445521E-17, 9.999999999997510880E-05 ),
 .UNSPECIFIED. ) ;
#41670=CARTESIAN_POINT ( 'NONE',  ( -0.5548696950099620828, -20.20177982057877841, 11.49999999999999645 ) ) ;
#41673=CARTESIAN_POINT ( 'NONE',  ( -65.58953762381672448, -23.47596703998600276, 11.44779298504227505 ) ) ;
#41675=CARTESIAN_POINT ( 'NONE',  ( -59.58953762381672448, -23.48786465467241058, 11.44779295918254824 ) ) ;
#41676=CARTESIAN_POINT ( 'NONE',  ( -31.58953762381671382, -23.48786465467240347, 11.44779295918255180 ) ) ;
#41677=CARTESIAN_POINT ( 'NONE',  ( -39.62287095715004881, -23.48783264082477373, -1.443836473390072594 ) ) ;
#41678=CARTESIAN_POINT ( 'NONE',  ( -81.62287095715005592, -24.65952944569304606, 1.056160979905699460 ) ) ;
#41679=CARTESIAN_POINT ( 'NONE',  ( 18.22975119132022215, -8.346483668847822557, -1.500000000000002220 ) ) ;
#41680=EDGE_CURVE ( 'NONE', #86931, #3899, #21541, .T. ) ;
#41682=ORIENTED_EDGE ( 'NONE', *, *, #1818, .T. ) ;
#41686=CARTESIAN_POINT ( 'NONE',  ( -35.58103620899936459, -24.73486907724918282, 1.287355809206967461 ) ) ;
#41687=CARTESIAN_POINT ( 'NONE',  ( -79.34687923781920915, -25.26778825442007559, 5.960409282772108241 ) ) ;
#41689=CARTESIAN_POINT ( 'NONE',  ( -101.0647859952741783, -25.13441618929300603, 2.968838638867928648 ) ) ;
#41692=LINE ( 'NONE', #10728, #5736 ) ;
#41693=CARTESIAN_POINT ( 'NONE',  ( -99.90680059161346094, -25.20650842489795807, 6.812665538484692362 ) ) ;
#41695=AXIS2_PLACEMENT_3D ( 'NONE', #8660, #30986, #91882 ) ;
#41696=CARTESIAN_POINT ( 'NONE',  ( -13.46841296510753061, 15.22696965993213070, -1.500000000000002220 ) ) ;
#41698=ADVANCED_FACE ( 'NONE', ( #99169 ), #84836, .T. ) ;
#41700=CARTESIAN_POINT ( 'NONE',  ( -127.5564499832624108, -23.48786465467242124, 11.44779295918253226 ) ) ;
#41702=CARTESIAN_POINT ( 'NONE',  ( -105.6228709571500559, -24.63287334234180292, 0.9662140553045504010 ) ) ;
#41704=CARTESIAN_POINT ( 'NONE',  ( -49.74873825466967503, -25.26264143758006142, 6.941713674697326475 ) ) ;
#41706=CARTESIAN_POINT ( 'NONE',  ( -9.521469661382619520, 18.92286876745961166, 11.49999999999999645 ) ) ;
#41707=CARTESIAN_POINT ( 'NONE',  ( -14.81638660137672225, 16.44347145309322045, 11.49999999999998934 ) ) ;
#41709=CARTESIAN_POINT ( 'NONE',  ( -1.637206367458305500, 20.51943892441452633, 11.49999999999998934 ) ) ;
#41710=B_SPLINE_CURVE_WITH_KNOTS ( 'NONE', 3,
 ( #94864, #1021, #94364, #64455 ),
 .UNSPECIFIED., .F., .F.,
 ( 4, 4 ),
 ( 0.000000000000000000, 9.999999999997510880E-05 ),
 .UNSPECIFIED. ) ;
#41711=ORIENTED_EDGE ( 'NONE', *, *, #79429, .F. ) ;
#41712=CARTESIAN_POINT ( 'NONE',  ( -113.5895376238167245, -23.47596703998600631, 11.44779298504227683 ) ) ;
#41715=DIRECTION ( 'NONE',  ( 0.000000000000000000, -2.173523156925979552E-06, 0.9999999999976378895 ) ) ;
#41718=ORIENTED_EDGE ( 'NONE', *, *, #43698, .T. ) ;
#41719=CARTESIAN_POINT ( 'NONE',  ( -116.6228709571500275, -23.47596703998600631, 11.44779298504227860 ) ) ;
#41722=CARTESIAN_POINT ( 'NONE',  ( -20.55201672899488585, 2.666056886502145673, -1.500000000000002220 ) ) ;
#41723=CARTESIAN_POINT ( 'NONE',  ( -20.56447267657262401, 6.860157381912782348, 11.49999999999999645 ) ) ;
#41725=CARTESIAN_POINT ( 'NONE',  ( -94.52287095715006160, -23.48786465467242479, 11.44779295918254292 ) ) ;
#41726=AXIS2_PLACEMENT_3D ( 'NONE', #88409, #34626, #57475 ) ;
#41727=LINE ( 'NONE', #20349, #40016 ) ;
#41728=CARTESIAN_POINT ( 'NONE',  ( 10.13505985054399083, -19.98934331558005439, 11.49999999999998934 ) ) ;
#41729=CARTESIAN_POINT ( 'NONE',  ( -110.9909297185884327, -25.14264188228929697, 6.986250900936915365 ) ) ;
#41730=FACE_OUTER_BOUND ( 'NONE', #40808, .T. ) ;
#41731=VERTEX_POINT ( 'NONE', #55519 ) ;
#41733=DIRECTION ( 'NONE',  ( 0.000000000000000000, -2.173523156925979552E-06, 0.9999999999976378895 ) ) ;
#41734=B_SPLINE_SURFACE_WITH_KNOTS ( 'NONE', 3, 1, ( 
 ( #71268, #79867 ),
 ( #87488, #47933 ),
 ( #48437, #25078 ),
 ( #32695, #17978 ),
 ( #63166, #10360 ),
 ( #85479, #46930 ),
 ( #70265, #749 ),
 ( #31702, #40317 ),
 ( #9356, #62668 ),
 ( #63677, #24079 ),
 ( #55048, #70767 ),
 ( #47432, #8861 ),
 ( #1263, #94597 ),
 ( #67165, #88494 ),
 ( #50934, #81872 ),
 ( #20457, #97591 ),
 ( #51430, #58546 ),
 ( #97098, #65679 ),
 ( #4752, #66680 ) ),
 .UNSPECIFIED., .F., .F., .F.,
 ( 4, 1, 1, 1, 1, 1, 1, 1, 1, 1, 1, 1, 1, 1, 1, 1, 4 ),
 ( 2, 2 ),
 ( 0.000000000000000000, 0.05090243768365541877, 0.1010340427826159765, 0.1510838170086600818, 0.2030619875551388231, 0.2562484343627552397, 0.3108467145046008295, 0.3687690999693260530, 0.4300150403860056869, 0.4925196472738457842, 0.5560487215256794125, 0.6219956829149523303, 0.6901923690829533387, 0.7613848549885010586, 0.8363562199507234007, 0.9154870053271095820, 1.000000000000000000 ),
 ( 0.000000000000000000, 1.000000000000000000 ),
 .UNSPECIFIED. ) ;
#41735=ORIENTED_EDGE ( 'NONE', *, *, #47982, .T. ) ;
#41736=VERTEX_POINT ( 'NONE', #77817 ) ;
#41737=CARTESIAN_POINT ( 'NONE',  ( -46.59348642383254457, -24.15620529776627379, 10.23563542870660825 ) ) ;
#41739=DIRECTION ( 'NONE',  ( 0.000000000000000000, 0.9999999999976377785, 2.173523156925978705E-06 ) ) ;
#41740=CARTESIAN_POINT ( 'NONE',  ( -4.916304867406160461, -20.68799595667769964, -1.500000000000002220 ) ) ;
#41741=ORIENTED_EDGE ( 'NONE', *, *, #73062, .F. ) ;
#41744=CARTESIAN_POINT ( 'NONE',  ( -19.11951126197014261, -10.51958540666066533, -1.500000000000002220 ) ) ;
#41745=DIRECTION ( 'NONE',  ( 0.000000000000000000, 2.173523156925980399E-06, -0.9999999999976378895 ) ) ;
#41746=CARTESIAN_POINT ( 'NONE',  ( -71.52287095715007581, -23.47596703998600631, 11.44779298504228748 ) ) ;
#41747=CARTESIAN_POINT ( 'NONE',  ( -85.62287095715004170, -29.50248789122583659, 2.256150453626215580 ) ) ;
#41748=CARTESIAN_POINT ( 'NONE',  ( -9.708950231915746798, -19.59419465507263070, -1.500000000000002220 ) ) ;
#41752=CARTESIAN_POINT ( 'NONE',  ( -85.50394113191364909, -24.52399227489127043, 9.353111116836526406 ) ) ;
#41753=VECTOR ( 'NONE', #57616, 1000.000000000000114 ) ;
#41756=VERTEX_POINT ( 'NONE', #7318 ) ;
#41757=CARTESIAN_POINT ( 'NONE',  ( -88.62287095715004170, -29.50247984919015209, -1.443849546365051806 ) ) ;
#41759=CARTESIAN_POINT ( 'NONE',  ( 3.248270302591931724, 20.98854991013365279, 11.49999999999998934 ) ) ;
#41761=CARTESIAN_POINT ( 'NONE',  ( -130.5728709571501440, -23.87624887660337691, 11.01174216661999772 ) ) ;
#41764=CARTESIAN_POINT ( 'NONE',  ( -68.54924039429016602, -24.15543982623907127, -0.2315651400026649820 ) ) ;
#41765=CARTESIAN_POINT ( 'NONE',  ( -12.45040968399260883, -14.89389333286084671, -1.500000000000002220 ) ) ;
#41766=CARTESIAN_POINT ( 'NONE',  ( -45.58529216989418131, -24.63355581998384736, 0.9682620441944017609 ) ) ;
#41769=CARTESIAN_POINT ( 'NONE',  ( -0.9579564967699066846, 19.55851204243107233, 11.49999999999999645 ) ) ;
#41774=VERTEX_POINT ( 'NONE', #24044 ) ;
#41776=CARTESIAN_POINT ( 'NONE',  ( -97.62287095715005592, -23.47593901973091235, -1.443836447539001089 ) ) ;
#41777=DIRECTION ( 'NONE',  ( 0.000000000000000000, 0.9999999999976377785, 2.173523156925979975E-06 ) ) ;
#41779=PLANE ( 'NONE',  #19615 ) ;
#41781=CARTESIAN_POINT ( 'NONE',  ( 13.13437215454093199, 14.66711140016434278, 11.49999999999998934 ) ) ;
#41782=ORIENTED_EDGE ( 'NONE', *, *, #93875, .F. ) ;
#41784=CARTESIAN_POINT ( 'NONE',  ( -8.701767255460435280, 21.38705905713849020, -1.500000000000002220 ) ) ;
#41787=ADVANCED_FACE ( 'NONE', ( #31660 ), #72510, .T. ) ;
#41791=CARTESIAN_POINT ( 'NONE',  ( -92.62287095715008434, -23.96127896941632685, -0.6493128931037810414 ) ) ;
#41792=CARTESIAN_POINT ( 'NONE',  ( -97.50897550903059141, -24.51419770103157703, 9.386484678747176957 ) ) ;
#41796=CARTESIAN_POINT ( 'NONE',  ( 19.92730240972663935, 0.8534881809820089593, 11.49999999999998934 ) ) ;
#41797=CARTESIAN_POINT ( 'NONE',  ( -75.53786448191598879, -24.83644354573578994, 8.397322867130100121 ) ) ;
#41798=CARTESIAN_POINT ( 'NONE',  ( 19.88832268942539017, -0.5522253751840191516, -1.500000000000002220 ) ) ;
#41799=VERTEX_POINT ( 'NONE', #49915 ) ;
#41800=AXIS2_PLACEMENT_3D ( 'NONE', #14639, #9032, #39983 ) ;
#41801=CARTESIAN_POINT ( 'NONE',  ( -122.5228709571500758, -24.50321055353805733, 9.387540953477520489 ) ) ;
#41802=CARTESIAN_POINT ( 'NONE',  ( -125.5228709571500616, -24.99132157543084531, 2.256160258750667502 ) ) ;
#41804=CARTESIAN_POINT ( 'NONE',  ( -80.53777078880429485, -24.92592662359561118, 8.075495903017996469 ) ) ;
#41805=CARTESIAN_POINT ( 'NONE',  ( -4.307737697753418082, 20.33289072680551968, 11.49999999999999645 ) ) ;
#41806=CARTESIAN_POINT ( 'NONE',  ( -38.52287095715006870, -23.47593901973090169, -1.443836447538997092 ) ) ;
#41807=CARTESIAN_POINT ( 'NONE',  ( -50.45700478961177993, -25.18512690614146265, 3.295337589435844539 ) ) ;
#41808=CARTESIAN_POINT ( 'NONE',  ( -2.521034868938843765, 22.70145277337256218, 11.49999999999999645 ) ) ;
#41810=B_SPLINE_SURFACE_WITH_KNOTS ( 'NONE', 3, 3, ( 
 ( #31478, #16254, #1032, #15750 ),
 ( #15247, #29, #16745, #47212 ),
 ( #78630, #40603, #32481, #63454 ),
 ( #40096, #94375, #71050, #39591 ),
 ( #55835, #86763, #70543, #46203 ),
 ( #17251, #53828, #48218, #31981 ),
 ( #62949, #39085, #47717, #32990 ) ),
 .UNSPECIFIED., .F., .F., .F.,
 ( 4, 3, 4 ),
 ( 4, 4 ),
 ( 0.7945040050992238090, 0.8970133687736495665, 0.9995227324480753239 ),
 ( 0.1195243700447448237, 0.1205922749804624466 ),
 .UNSPECIFIED. ) ;
#41811=DIRECTION ( 'NONE',  ( 0.000000000000000000, 0.9999999999976377785, 2.173523156925979128E-06 ) ) ;
#41813=ORIENTED_EDGE ( 'NONE', *, *, #51980, .F. ) ;
#41814=CARTESIAN_POINT ( 'NONE',  ( -14.69473627950705108, 13.90061564059656440, 11.49999999999998934 ) ) ;
#41820=VERTEX_POINT ( 'NONE', #1725 ) ;
#41821=CARTESIAN_POINT ( 'NONE',  ( -78.94507867893470632, -25.28412234718345530, 5.882162795622602580 ) ) ;
#41822=CARTESIAN_POINT ( 'NONE',  ( -51.29687923781917647, -25.27420715122566364, 3.993462153431225570 ) ) ;
#41823=CARTESIAN_POINT ( 'NONE',  ( -19.32702923155483177, -5.217993511516596961, -1.500000000000002220 ) ) ;
#41824=CARTESIAN_POINT ( 'NONE',  ( 9.933205088616889000, -18.45388779576350302, 11.49999999999999645 ) ) ;
#41827=CARTESIAN_POINT ( 'NONE',  ( 16.78392297789021015, 14.29496084597832883, -1.500000000000002220 ) ) ;
#41828=EDGE_CURVE ( 'NONE', #68707, #19712, #3243, .T. ) ;
#41829=VECTOR ( 'NONE', #30084, 1000.000000000000114 ) ;
#41830=CARTESIAN_POINT ( 'NONE',  ( -39.65036112522632550, -25.31589258738599568, 4.754946542694897360 ) ) ;
#41831=ORIENTED_EDGE ( 'NONE', *, *, #23311, .T. ) ;
#41832=DIRECTION ( 'NONE',  ( 0.000000000000000000, -0.9999999999976377785, -2.173523156925979975E-06 ) ) ;
#41833=DIRECTION ( 'NONE',  ( 3.773278334444166432E-23, -1.000000000000000000, 0.000000000000000000 ) ) ;
#41836=CARTESIAN_POINT ( 'NONE',  ( -51.62287095715005592, -29.50250243563736774, 8.947779886222146928 ) ) ;
#41839=VERTEX_POINT ( 'NONE', #2234 ) ;
#41841=CARTESIAN_POINT ( 'NONE',  ( -100.8972602205940063, -25.27404646237970454, 2.905315430698961698 ) ) ;
#41842=PLANE ( 'NONE',  #35796 ) ;
#41843=CARTESIAN_POINT ( 'NONE',  ( -14.05295919346176170, -14.94737400546395456, -1.500000000000002220 ) ) ;
#41844=ORIENTED_EDGE ( 'NONE', *, *, #48010, .T. ) ;
#41847=CARTESIAN_POINT ( 'NONE',  ( -96.52287095715001897, -24.66019654487199730, 8.947790411086115725 ) ) ;
#41848=CARTESIAN_POINT ( 'NONE',  ( -21.40455707349245529, -6.346402434563959361, 11.49999999999998934 ) ) ;
#41849=B_SPLINE_CURVE_WITH_KNOTS ( 'NONE', 3,
 ( #78500, #86627, #62817, #25223 ),
 .UNSPECIFIED., .F., .F.,
 ( 4, 4 ),
 ( 0.3207290247458886023, 0.3297354560180041361 ),
 .UNSPECIFIED. ) ;
#41850=CARTESIAN_POINT ( 'NONE',  ( -0.05083659990941528928, -22.39188026470795378, 1.363349870542274189 ) ) ;
#41851=CARTESIAN_POINT ( 'NONE',  ( -122.5228709571500616, -23.47596703998600631, 11.44779298504227860 ) ) ;
#41853=CARTESIAN_POINT ( 'NONE',  ( -101.6228709571500559, -24.65952944569304606, 1.056160979905702790 ) ) ;
#41856=CARTESIAN_POINT ( 'NONE',  ( -17.86878485216894319, -10.78119150571587781, 11.49999999999998934 ) ) ;
#41858=PLANE ( 'NONE',  #91134 ) ;
#41859=EDGE_LOOP ( 'NONE', ( #91262, #48916, #18245, #98413 ) ) ;
#41860=ORIENTED_EDGE ( 'NONE', *, *, #22270, .F. ) ;
#41862=CARTESIAN_POINT ( 'NONE',  ( 20.56459456670464547, 4.482388377596099538, -1.500000000000002220 ) ) ;
#41864=CARTESIAN_POINT ( 'NONE',  ( -95.62287095715005592, -23.47593901973091235, -1.443836447539001089 ) ) ;
#41865=DIRECTION ( 'NONE',  ( -3.773278334453079618E-23, 0.9999999999976377785, 2.173523156925979975E-06 ) ) ;
#41866=CARTESIAN_POINT ( 'NONE',  ( -120.6258260306066745, -24.40133493613049964, 9.663955038902800609 ) ) ;
#41867=CARTESIAN_POINT ( 'NONE',  ( -101.4365978186105366, -25.03152376165066073, 7.227289064697279386 ) ) ;
#41868=CARTESIAN_POINT ( 'NONE',  ( -129.6228709571500417, -24.64965695001463430, 8.947790411086117501 ) ) ;
#41869=CARTESIAN_POINT ( 'NONE',  ( -20.76051858633888259, -6.224802954461835292, -1.500000000000002220 ) ) ;
#41870=CARTESIAN_POINT ( 'NONE',  ( -79.99654428403167117, -25.05785469192115045, 7.493821146766848074 ) ) ;
#41871=CARTESIAN_POINT ( 'NONE',  ( -15.91109736606077441, 15.52988587838853540, 11.49999999999999645 ) ) ;
#41873=CARTESIAN_POINT ( 'NONE',  ( -51.19842764437002813, -25.31441786624639079, 5.493892295348231869 ) ) ;
#41874=CARTESIAN_POINT ( 'NONE',  ( -100.6814946224345846, -25.30267106336103922, 4.736250553104468963 ) ) ;
#41876=ORIENTED_EDGE ( 'NONE', *, *, #39827, .F. ) ;
#41877=CARTESIAN_POINT ( 'NONE',  ( -76.62287095715007013, -23.72747288104442021, -1.053458166803662444 ) ) ;
#41882=B_SPLINE_CURVE_WITH_KNOTS ( 'NONE', 3,
 ( #47687, #45305, #29561, #83850, #76226, #24336 ),
 .UNSPECIFIED., .F., .F.,
 ( 4, 2, 4 ),
 ( 0.000000000000000000, 0.001380764517853247733, 0.002761529035706495466 ),
 .UNSPECIFIED. ) ;
#41883=CARTESIAN_POINT ( 'NONE',  ( -107.5228709571501327, -23.96127896942120827, -0.6493128930941749477 ) ) ;
#41884=CARTESIAN_POINT ( 'NONE',  ( -51.52287095715006870, -23.47596703998600631, 11.44779298504229104 ) ) ;
#41885=ORIENTED_EDGE ( 'NONE', *, *, #96389, .F. ) ;
#41886=EDGE_CURVE ( 'NONE', #10916, #95349, #30055, .T. ) ;
#41887=CARTESIAN_POINT ( 'NONE',  ( -130.5728709571500588, -24.85767102478814650, 1.377180730259818908 ) ) ;
#41888=CARTESIAN_POINT ( 'NONE',  ( -13.02831144489870319, 18.26546089674541307, -1.500000000000002220 ) ) ;
#41891=CARTESIAN_POINT ( 'NONE',  ( -89.40841769935769889, -25.23397913219577049, 6.409327625469732226 ) ) ;
#41892=CARTESIAN_POINT ( 'NONE',  ( -101.6251895264811225, -24.51419770103158413, 9.386484678747175181 ) ) ;
#41893=ADVANCED_FACE ( 'NONE', ( #71238 ), #72240, .F. ) ;
#41894=CARTESIAN_POINT ( 'NONE',  ( -98.62287095715005592, -29.50250786944525672, 11.44777988621623166 ) ) ;
#41896=AXIS2_PLACEMENT_3D ( 'NONE', #7447, #48030, #85075 ) ;
#41898=CARTESIAN_POINT ( 'NONE',  ( -30.57310282152668890, -25.30559561715417516, 6.147794833475641596 ) ) ;
#41899=CARTESIAN_POINT ( 'NONE',  ( 17.47348308817029405, 8.859467055162037141, -1.500000000000002220 ) ) ;
#41903=CARTESIAN_POINT ( 'NONE',  ( -19.98823316618875268, 7.996883007359760320, 11.49999999999998934 ) ) ;
#41905=EDGE_CURVE ( 'NONE', #14276, #35568, #71239, .T. ) ;
#41907=PLANE ( 'NONE',  #84679 ) ;
#41908=CARTESIAN_POINT ( 'NONE',  ( -128.6228709571500417, -23.48786465467242479, 11.44779295918253403 ) ) ;
#41909=CARTESIAN_POINT ( 'NONE',  ( -5.713817535623205046, 22.21719745612757535, -1.500000000000002220 ) ) ;
#41911=DIRECTION ( 'NONE',  ( -3.773278334453079618E-23, 0.9999999999976377785, 2.173523156925979975E-06 ) ) ;
#41912=CARTESIAN_POINT ( 'NONE',  ( -49.50711149851015591, -23.96119346886879953, -0.6495511937832113558 ) ) ;
#41913=CARTESIAN_POINT ( 'NONE',  ( 10.01938154005162218, -17.43019892170380913, 11.49999999999999645 ) ) ;
#41914=CARTESIAN_POINT ( 'NONE',  ( -109.8914236385200525, -25.10927407888622653, 2.885852620966828042 ) ) ;
#41918=CARTESIAN_POINT ( 'NONE',  ( -65.62287095715008434, -24.14321612903114556, -0.2833117244521677347 ) ) ;
#41919=EDGE_CURVE ( 'NONE', #62726, #92355, #61534, .T. ) ;
#41920=FACE_OUTER_BOUND ( 'NONE', #96262, .T. ) ;
#41921=CARTESIAN_POINT ( 'NONE',  ( -19.81728208556213389, 0.3677575464312098363, 11.49999999999998934 ) ) ;
#41922=PLANE ( 'NONE',  #22089 ) ;
#41923=CARTESIAN_POINT ( 'NONE',  ( -19.65353550717971487, 1.628721094194526486, -1.500000000000002220 ) ) ;
#41924=CARTESIAN_POINT ( 'NONE',  ( -60.58953762381671737, -23.48783264082478439, -1.443836473390068820 ) ) ;
#41925=AXIS2_PLACEMENT_3D ( 'NONE', #1233, #31164, #86956 ) ;
#41927=DIRECTION ( 'NONE',  ( -1.000000000000000000, -3.773278334444166432E-23, -8.201307841325785021E-29 ) ) ;
#41929=CARTESIAN_POINT ( 'NONE',  ( 20.22723401096548201, -3.897675682603606084, 11.49999999999999645 ) ) ;
#41931=B_SPLINE_CURVE_WITH_KNOTS ( 'NONE', 3,
 ( #34603, #49841, #94487, #65574 ),
 .UNSPECIFIED., .F., .F.,
 ( 4, 4 ),
 ( 0.000000000000000000, 9.999999999998897304E-05 ),
 .UNSPECIFIED. ) ;
#41932=CARTESIAN_POINT ( 'NONE',  ( 10.43192878459595185, 20.09917060401269850, 11.49999999999999645 ) ) ;
#41933=ORIENTED_EDGE ( 'NONE', *, *, #28038, .F. ) ;
#41934=CARTESIAN_POINT ( 'NONE',  ( -69.34542366606198982, -25.25639427084792032, 6.299234904174134897 ) ) ;
#41935=CARTESIAN_POINT ( 'NONE',  ( -109.6228709571501128, -24.33927499327855415, 9.819080762295815390 ) ) ;
#41936=EDGE_CURVE ( 'NONE', #90373, #59480, #95567, .T. ) ;
#41938=CARTESIAN_POINT ( 'NONE',  ( -36.58953762381672448, -23.48783264082477729, -1.443836473390072372 ) ) ;
#41941=ORIENTED_EDGE ( 'NONE', *, *, #90910, .F. ) ;
#41942=CARTESIAN_POINT ( 'NONE',  ( -79.89247415061277025, -25.26749899421020373, 5.073623479721068641 ) ) ;
#41943=CARTESIAN_POINT ( 'NONE',  ( -7.631545101075025705, 21.52643039700453897, -1.500000000000002220 ) ) ;
#41946=CARTESIAN_POINT ( 'NONE',  ( -82.51327497436713543, -23.96169478059713143, 10.65365249895718414 ) ) ;
#41947=CARTESIAN_POINT ( 'NONE',  ( -12.88509029660790617, -18.40938060607246740, 11.49999999999999645 ) ) ;
#41949=CARTESIAN_POINT ( 'NONE',  ( -36.58953762381671737, -23.47596703998600276, 11.44779298504227505 ) ) ;
#41950=CARTESIAN_POINT ( 'NONE',  ( -18.27885182143903720, 12.20952002138517045, -1.500000000000002220 ) ) ;
#41951=FACE_OUTER_BOUND ( 'NONE', #99815, .T. ) ;
#41953=CARTESIAN_POINT ( 'NONE',  ( -69.62287095715005592, -29.50250786944525672, 11.44777988621623699 ) ) ;
#41955=CARTESIAN_POINT ( 'NONE',  ( -71.52287095715010423, -23.48783264082477018, -1.443836473390091246 ) ) ;
#41956=EDGE_CURVE ( 'NONE', #3335, #12512, #74813, .T. ) ;
#41959=CARTESIAN_POINT ( 'NONE',  ( -103.5228709571501042, -23.48783264082477018, -1.443836473390087916 ) ) ;
#41961=CARTESIAN_POINT ( 'NONE',  ( -11.60840874443078263, -16.91462557209307960, 11.49999999999998934 ) ) ;
#41962=ORIENTED_EDGE ( 'NONE', *, *, #82237, .T. ) ;
#41966=DIRECTION ( 'NONE',  ( -3.773278334453079030E-23, 0.9999999999976377785, 2.173523156925979128E-06 ) ) ;
#41967=CARTESIAN_POINT ( 'NONE',  ( 6.977686149863070675, -22.03694335537135984, 11.49999999999998934 ) ) ;
#41968=CARTESIAN_POINT ( 'NONE',  ( -104.5117914961601713, -24.51419770103158768, 9.386484678747166299 ) ) ;
#41969=CARTESIAN_POINT ( 'NONE',  ( -18.82316870354832616, 7.800066519331792847, -1.500000000000002220 ) ) ;
#41970=ADVANCED_FACE ( 'NONE', ( #25046 ), #79335, .T. ) ;
#41971=ORIENTED_EDGE ( 'NONE', *, *, #41314, .F. ) ;
#41976=CARTESIAN_POINT ( 'NONE',  ( -71.66734858977571321, -25.25855161950308769, 6.551008370017044058 ) ) ;
#41978=CARTESIAN_POINT ( 'NONE',  ( -29.17364183714287762, -25.21531997571052486, 3.835940394522498575 ) ) ;
#41979=CARTESIAN_POINT ( 'NONE',  ( -93.52287095715007581, -24.50321055353807154, 9.387540953477520489 ) ) ;
#41982=CARTESIAN_POINT ( 'NONE',  ( -4.307737697753418082, 20.33289072680551968, -1.500000000000002220 ) ) ;
#41985=CARTESIAN_POINT ( 'NONE',  ( -125.5888994550898303, -24.92564183028979485, 1.928384488918254425 ) ) ;
#41986=VERTEX_POINT ( 'NONE', #96072 ) ;
#41987=B_SPLINE_CURVE_WITH_KNOTS ( 'NONE', 3,
 ( #24508, #55478, #86414, #71702 ),
 .UNSPECIFIED., .F., .F.,
 ( 4, 4 ),
 ( 0.000000000000000000, 9.999999999998897304E-05 ),
 .UNSPECIFIED. ) ;
#41988=CARTESIAN_POINT ( 'NONE',  ( -41.66427398439827812, -23.48786465467240347, 11.44779295918255180 ) ) ;
#41989=CARTESIAN_POINT ( 'NONE',  ( -102.6228709571500701, -24.50216790748099172, 0.6166512839513705879 ) ) ;
#41991=ORIENTED_EDGE ( 'NONE', *, *, #43217, .F. ) ;
#41992=DIRECTION ( 'NONE',  ( 0.000000000000000000, 0.9999999999976377785, 2.173523156925979128E-06 ) ) ;
#41993=B_SPLINE_CURVE_WITH_KNOTS ( 'NONE', 3,
 ( #49253, #34512, #80180, #65484, #26892, #72084 ),
 .UNSPECIFIED., .F., .F.,
 ( 4, 2, 4 ),
 ( 1.570887131794638196E-05, 0.001396322306279761073, 0.002776935741241575838 ),
 .UNSPECIFIED. ) ;
#41996=B_SPLINE_CURVE_WITH_KNOTS ( 'NONE', 3,
 ( #10605, #55299, #33947, #26334, #3505, #10105, #64926, #71016, #25328, #1507, #9103, #88239, #41063, #34449 ),
 .UNSPECIFIED., .F., .F.,
 ( 4, 2, 2, 2, 2, 2, 4 ),
 ( 0.000000000000000000, 0.0001952411637358899145, 0.0003904823274717798289, 0.0007809646549435615009, 0.001171446982415343119, 0.001366688146151234145, 0.001561929309887125170 ),
 .UNSPECIFIED. ) ;
#41997=CARTESIAN_POINT ( 'NONE',  ( -71.10442080388585850, -25.31201661486003474, 5.639839434645662841 ) ) ;
#41998=CARTESIAN_POINT ( 'NONE',  ( 22.02032638543937182, 1.892999326154024553, 11.49999999999999645 ) ) ;
#41999=ORIENTED_EDGE ( 'NONE', *, *, #16602, .F. ) ;
#42001=CARTESIAN_POINT ( 'NONE',  ( -19.18631400275845422, -11.98935526391121087, -1.500000000000002220 ) ) ;
#42005=DIRECTION ( 'NONE',  ( -3.773278334444166432E-23, 1.000000000000000000, 0.000000000000000000 ) ) ;
#42007=EDGE_LOOP ( 'NONE', ( #24128, #18265, #79084, #15231 ) ) ;
#42008=CARTESIAN_POINT ( 'NONE',  ( -9.521469661382619520, 18.92286876745961166, 11.49999999999998934 ) ) ;
#42009=CARTESIAN_POINT ( 'NONE',  ( -78.95422500253870624, -25.03138002232442005, 6.195241297245855705 ) ) ;
#42011=FACE_OUTER_BOUND ( 'NONE', #24986, .T. ) ;
#42012=CARTESIAN_POINT ( 'NONE',  ( 0.7529269182969693386, -22.20201975079678647, -1.500000000000002220 ) ) ;
#42013=CARTESIAN_POINT ( 'NONE',  ( -49.25033725972690490, -25.03220807947403515, 7.108518685806449966 ) ) ;
#42014=EDGE_CURVE ( 'NONE', #47218, #27337, #967, .T. ) ;
#42015=EDGE_LOOP ( 'NONE', ( #43565, #32173, #12916, #11215 ) ) ;
#42016=CARTESIAN_POINT ( 'NONE',  ( -79.62287095715004170, -23.47596703998600631, 11.44779298504227860 ) ) ;
#42017=CARTESIAN_POINT ( 'NONE',  ( -104.5228709571500758, -23.47593901973090524, -1.443836447538996204 ) ) ;
#42018=CARTESIAN_POINT ( 'NONE',  ( -36.54573691098784849, -24.15620529776627379, 10.23563542870660825 ) ) ;
#42020=CARTESIAN_POINT ( 'NONE',  ( -14.34788840963776124, 13.16932220997287928, -1.500000000000002220 ) ) ;
#42022=CARTESIAN_POINT ( 'NONE',  ( 9.988417798295188277, 18.97302403871600518, 11.49999999999998934 ) ) ;
#42023=CARTESIAN_POINT ( 'NONE',  ( -27.26447433122779884, -24.92774676623168162, 1.676004566348860525 ) ) ;
#42024=B_SPLINE_CURVE_WITH_KNOTS ( 'NONE', 3,
 ( #80962, #73357, #41918, #95687, #26172, #27180, #81470, #65762 ),
 .UNSPECIFIED., .F., .F.,
 ( 4, 2, 2, 4 ),
 ( 0.000000000000000000, 0.002001098010032689289, 0.003001647015049033716, 0.004002196020065378577 ),
 .UNSPECIFIED. ) ;
#42026=DIRECTION ( 'NONE',  ( -3.773278334453079618E-23, 0.9999999999976377785, 2.173523156925979975E-06 ) ) ;
#42027=CARTESIAN_POINT ( 'NONE',  ( -77.63398884115866849, -24.15543982623907482, -0.2315651400026658147 ) ) ;
#42028=CARTESIAN_POINT ( 'NONE',  ( -20.46125754976198508, 9.905080999540670561, -1.500000000000002220 ) ) ;
#42030=CARTESIAN_POINT ( 'NONE',  ( -98.55250747182638804, -24.15543982623907482, -0.2315651400026625395 ) ) ;
#42031=CARTESIAN_POINT ( 'NONE',  ( -119.5228709571500758, -29.50250786944525672, 11.44777988621622811 ) ) ;
#42032=CARTESIAN_POINT ( 'NONE',  ( 3.219775368129482285, -19.64489633315863770, 11.49999999999999645 ) ) ;
#42033=PLANE ( 'NONE',  #21156 ) ;
#42035=CARTESIAN_POINT ( 'NONE',  ( -39.54606421208372069, -24.15620529776627734, 10.23563542870661180 ) ) ;
#42036=CARTESIAN_POINT ( 'NONE',  ( -128.5562042904833788, -24.66019654487199730, 8.947790411086119278 ) ) ;
#42037=ORIENTED_EDGE ( 'NONE', *, *, #32238, .F. ) ;
#42038=EDGE_CURVE ( 'NONE', #27723, #53455, #20419, .T. ) ;
#42040=DIRECTION ( 'NONE',  ( -3.773278334453079030E-23, 0.9999999999976377785, 2.173523156925979128E-06 ) ) ;
#42041=CARTESIAN_POINT ( 'NONE',  ( 21.21565077533257337, 4.556159429511043690, -1.500000000000002220 ) ) ;
#42042=CARTESIAN_POINT ( 'NONE',  ( -84.52287095715010423, -23.73934037231757443, 11.05740245334329153 ) ) ;
#42044=CARTESIAN_POINT ( 'NONE',  ( 14.87128047407919951, 12.67365258641725312, -1.500000000000002220 ) ) ;
#42045=CARTESIAN_POINT ( 'NONE',  ( -93.52287095715011844, -24.51283580621364067, 0.6167428607019835862 ) ) ;
#42049=VECTOR ( 'NONE', #91442, 1000.000000000000114 ) ;
#42050=DIRECTION ( 'NONE',  ( -3.773278334453080206E-23, 0.9999999999976377785, 2.173523156925979975E-06 ) ) ;
#42051=CARTESIAN_POINT ( 'NONE',  ( -20.22731604866883970, -2.807383831903240257, 11.49999999999999645 ) ) ;
#42052=DIRECTION ( 'NONE',  ( -3.773278334453079030E-23, 0.9999999999976377785, 2.173523156925979128E-06 ) ) ;
#42057=CARTESIAN_POINT ( 'NONE',  ( -39.44943695351214785, -25.28892596830959505, 4.097884984622077731 ) ) ;
#42058=FACE_OUTER_BOUND ( 'NONE', #75813, .T. ) ;
#42059=FACE_OUTER_BOUND ( 'NONE', #33310, .T. ) ;
#42060=ORIENTED_EDGE ( 'NONE', *, *, #28431, .F. ) ;
#42061=LINE ( 'NONE', #94323, #54437 ) ;
#42063=CARTESIAN_POINT ( 'NONE',  ( -18.54830753475928518, 13.48922247889305837, 11.49999999999999645 ) ) ;
#42064=CARTESIAN_POINT ( 'NONE',  ( 2.720868037236281012, -22.60253418658637869, -1.500000000000002220 ) ) ;
#42067=CARTESIAN_POINT ( 'NONE',  ( -90.58606721154154684, -24.73486907724917572, 1.287355809206966573 ) ) ;
#42068=CARTESIAN_POINT ( 'NONE',  ( -74.52287095715010423, -24.35013146730203815, 9.818937971375095941 ) ) ;
#42069=CARTESIAN_POINT ( 'NONE',  ( -69.86226356453386188, -25.11033435731149055, 2.832404375966413479 ) ) ;
#42070=CARTESIAN_POINT ( 'NONE',  ( -20.59625928752216240, -7.366027188055905839, 11.49999999999998934 ) ) ;
#42073=EDGE_CURVE ( 'NONE', #96286, #33243, #50568, .T. ) ;
#42074=CARTESIAN_POINT ( 'NONE',  ( -26.09950754783970339, -24.95550736417008508, 4.652252430823455853 ) ) ;
#42075=CARTESIAN_POINT ( 'NONE',  ( -71.70841769935766763, -25.24715640642683923, 6.192981443001071895 ) ) ;
#42076=CARTESIAN_POINT ( 'NONE',  ( -58.50334559872716511, -24.15543982623907482, -0.2315651400026660645 ) ) ;
#42077=ORIENTED_EDGE ( 'NONE', *, *, #47858, .F. ) ;
#42078=CARTESIAN_POINT ( 'NONE',  ( -19.05221060042639536, -7.346018566486852031, 11.49999999999998934 ) ) ;
#42080=ORIENTED_EDGE ( 'NONE', *, *, #9310, .F. ) ;
#42082=CARTESIAN_POINT ( 'NONE',  ( -1.485350438481424895, -22.96994831426971828, 11.49999999999998934 ) ) ;
#42083=LINE ( 'NONE', #89743, #42196 ) ;
#42084=CARTESIAN_POINT ( 'NONE',  ( 20.15506735835773000, -1.303320585059813741, -1.500000000000002220 ) ) ;
#42087=LINE ( 'NONE', #50687, #6100 ) ;
#42089=CARTESIAN_POINT ( 'NONE',  ( -123.5895376238167245, -23.47593901973091235, -1.443836447538997536 ) ) ;
#42090=CARTESIAN_POINT ( 'NONE',  ( 16.24497012180664868, 13.92215130028523973, 11.49999999999999645 ) ) ;
#42092=DIRECTION ( 'NONE',  ( 0.7296913851534244655, -1.486204343759023298E-06, 0.6837766319717778485 ) ) ;
#42094=CARTESIAN_POINT ( 'NONE',  ( -7.755428854246955161, -20.87388092083558888, 11.49999999999998934 ) ) ;
#42095=CARTESIAN_POINT ( 'NONE',  ( 12.06641648444584369, 16.80774221200798735, -1.500000000000002220 ) ) ;
#42097=EDGE_CURVE ( 'NONE', #27790, #16362, #10674, .T. ) ;
#42098=B_SPLINE_CURVE_WITH_KNOTS ( 'NONE', 3,
 ( #48837, #4154, #81770, #65577 ),
 .UNSPECIFIED., .F., .F.,
 ( 4, 4 ),
 ( 0.000000000000000000, 9.999999999999592548E-05 ),
 .UNSPECIFIED. ) ;
#42101=CARTESIAN_POINT ( 'NONE',  ( -68.92786316032828609, -25.03707830618030172, 7.590867772707288630 ) ) ;
#42103=CARTESIAN_POINT ( 'NONE',  ( -81.52287095715007581, -24.51283580621452884, 0.6167428607046336886 ) ) ;
#42104=VERTEX_POINT ( 'NONE', #81841 ) ;
#42106=CARTESIAN_POINT ( 'NONE',  ( 2.313481123293766206, -20.83243486019555135, -1.500000000000002220 ) ) ;
#42107=B_SPLINE_CURVE_WITH_KNOTS ( 'NONE', 3,
 ( #83688, #36017, #53758, #46140, #83181, #13665 ),
 .UNSPECIFIED., .F., .F.,
 ( 4, 2, 4 ),
 ( 0.000000000000000000, 0.001380901958385383124, 0.002761803916770766247 ),
 .UNSPECIFIED. ) ;
#42108=CARTESIAN_POINT ( 'NONE',  ( -16.46405638241306946, -14.47283864684382237, 11.49999999999999645 ) ) ;
#42109=CARTESIAN_POINT ( 'NONE',  ( -73.53860178212968890, -24.66019654487200441, 8.947790411086119278 ) ) ;
#42110=CARTESIAN_POINT ( 'NONE',  ( -1.726696889551340153, 22.42386595106472669, 11.49999999999998934 ) ) ;
#42111=EDGE_CURVE ( 'NONE', #73872, #71528, #40859, .T. ) ;
#42114=CARTESIAN_POINT ( 'NONE',  ( 19.95448254803897115, -6.385634049875297258, 11.49999999999998934 ) ) ;
#42115=CARTESIAN_POINT ( 'NONE',  ( -27.70544111104076990, -29.50248652753305478, 1.628739237965270537 ) ) ;
#42116=CARTESIAN_POINT ( 'NONE',  ( -108.8968792378192063, -25.12726808145882629, 7.140617874877389859 ) ) ;
#42117=CARTESIAN_POINT ( 'NONE',  ( -91.55620429048339304, -24.64965694238574656, 8.947790433994201820 ) ) ;
#42122=AXIS2_PLACEMENT_3D ( 'NONE', #74099, #88828, #2596 ) ;
#42123=ORIENTED_EDGE ( 'NONE', *, *, #94048, .F. ) ;
#42124=CARTESIAN_POINT ( 'NONE',  ( -52.54749795293748349, -24.15543982623907482, -0.2315651400026529916 ) ) ;
#42126=B_SPLINE_CURVE_WITH_KNOTS ( 'NONE', 3,
 ( #87481, #49438, #40804, #73267 ),
 .UNSPECIFIED., .F., .F.,
 ( 4, 4 ),
 ( 0.000000000000000000, 0.0001000000000000028644 ),
 .UNSPECIFIED. ) ;
#42127=AXIS2_PLACEMENT_3D ( 'NONE', #66095, #34625, #43240 ) ;
#42128=CARTESIAN_POINT ( 'NONE',  ( -12.70309173801008562, -17.24390854791867511, -1.500000000000002220 ) ) ;
#42129=VERTEX_POINT ( 'NONE', #90448 ) ;
#42130=CARTESIAN_POINT ( 'NONE',  ( -26.19055979656421584, -24.92561770071717930, 6.008896093053317067 ) ) ;
#42131=CARTESIAN_POINT ( 'NONE',  ( 20.24497096899912307, 5.935080660949433096, 11.49999999999998934 ) ) ;
#42132=CARTESIAN_POINT ( 'NONE',  ( -30.61623571243587349, -24.27934583723679651, 9.960304333224314632 ) ) ;
#42134=CARTESIAN_POINT ( 'NONE',  ( -97.22287095715006444, -23.47596703998600631, 11.44779298504227860 ) ) ;
#42135=CARTESIAN_POINT ( 'NONE',  ( -80.35919894935767616, -25.30877072896627666, 4.505481309076929897 ) ) ;
#42136=CARTESIAN_POINT ( 'NONE',  ( -129.5899315912527356, -23.73791477778912906, 11.05961554403170233 ) ) ;
#42137=CARTESIAN_POINT ( 'NONE',  ( 2.156995527713877259, 21.93451973775924557, -1.500000000000002220 ) ) ;
#42139=CARTESIAN_POINT ( 'NONE',  ( -65.53230649573079347, -24.92592662359560762, 8.075495903017996469 ) ) ;
#42140=EDGE_CURVE ( 'NONE', #96582, #49194, #17851, .T. ) ;
#42142=CARTESIAN_POINT ( 'NONE',  ( -40.76794460738368997, -25.27956066610283870, 5.521532736733258950 ) ) ;
#42143=CARTESIAN_POINT ( 'NONE',  ( -62.61045561229671108, -23.48786465467241413, 11.44779295918255002 ) ) ;
#42144=CARTESIAN_POINT ( 'NONE',  ( -26.57444913475580250, -24.61859514035917584, 1.999156410758380575 ) ) ;
#42145=CARTESIAN_POINT ( 'NONE',  ( -102.5895376238167245, -23.47593901973091235, -1.443836447539001089 ) ) ;
#42146=CARTESIAN_POINT ( 'NONE',  ( 21.34331307443176584, 0.5271963136488534429, -1.500000000000002220 ) ) ;
#42147=FACE_OUTER_BOUND ( 'NONE', #100337, .T. ) ;
#42148=CARTESIAN_POINT ( 'NONE',  ( -50.92004226540860401, -25.20650842489795451, 6.812665538484691474 ) ) ;
#42149=ADVANCED_FACE ( 'NONE', ( #52392 ), #74229, .T. ) ;
#42150=CARTESIAN_POINT ( 'NONE',  ( -0.1490749075164066184, -21.12010817310450861, 11.44779298504228038 ) ) ;
#42152=CARTESIAN_POINT ( 'NONE',  ( -3.174168706971715270, 22.36591850054903929, -1.500000000000002220 ) ) ;
#42153=EDGE_CURVE ( 'NONE', #28343, #25435, #45710, .T. ) ;
#42155=VERTEX_POINT ( 'NONE', #53115 ) ;
#42156=PLANE ( 'NONE',  #35304 ) ;
#42157=CARTESIAN_POINT ( 'NONE',  ( -79.64187532455639484, -23.73766607897669800, -1.055555164236459564 ) ) ;
#42158=CARTESIAN_POINT ( 'NONE',  ( -10.80270875523330965, -16.48872379891551532, 11.49999999999999645 ) ) ;
#42159=CARTESIAN_POINT ( 'NONE',  ( -32.07722060962684196, -24.87479601683932984, 8.247789944617052171 ) ) ;
#42160=LINE ( 'NONE', #65504, #96578 ) ;
#42161=ORIENTED_EDGE ( 'NONE', *, *, #73259, .F. ) ;
#42164=CARTESIAN_POINT ( 'NONE',  ( -29.12854162637831834, -25.26026429949986607, 2.289899196687330551 ) ) ;
#42165=CARTESIAN_POINT ( 'NONE',  ( -101.1189062734182755, -25.17353303595478664, 6.916461067677506236 ) ) ;
#42166=CARTESIAN_POINT ( 'NONE',  ( 7.158504886898216846, -20.39052948596947346, -1.500000000000002220 ) ) ;
#42168=CARTESIAN_POINT ( 'NONE',  ( -13.40542139710017899, 13.98966777563825481, -1.500000000000002220 ) ) ;
#42169=ADVANCED_FACE ( 'NONE', ( #28768 ), #68830, .F. ) ;
#42171=DIRECTION ( 'NONE',  ( -3.773278334453079618E-23, 0.9999999999976377785, 2.173523156925978705E-06 ) ) ;
#42172=CARTESIAN_POINT ( 'NONE',  ( -15.09475962229707591, 12.77647934908296712, -1.500000000000002220 ) ) ;
#42174=CARTESIAN_POINT ( 'NONE',  ( 20.23688964843749005, 1.552196809742036221, 11.49999999999999645 ) ) ;
#42177=ORIENTED_EDGE ( 'NONE', *, *, #68320, .F. ) ;
#42183=CARTESIAN_POINT ( 'NONE',  ( -105.5228709571500758, -29.50247984919015209, -1.443849546365048253 ) ) ;
#42184=B_SPLINE_CURVE_WITH_KNOTS ( 'NONE', 3,
 ( #64729, #100347, #86151, #41874 ),
 .UNSPECIFIED., .F., .F.,
 ( 4, 4 ),
 ( 3.973137263842166252E-09, 0.0004615443969624879301 ),
 .UNSPECIFIED. ) ;
#42185=CARTESIAN_POINT ( 'NONE',  ( -71.62287095715005592, -23.47593901973091235, -1.443836447539006196 ) ) ;
#42186=CARTESIAN_POINT ( 'NONE',  ( 9.011679573027636891, 17.89655708981447901, 11.49999999999998934 ) ) ;
#42191=EDGE_CURVE ( 'NONE', #73900, #22592, #51612, .T. ) ;
#42196=VECTOR ( 'NONE', #95851, 1000.000000000000114 ) ;
#42197=CARTESIAN_POINT ( 'NONE',  ( -105.5228709571500900, -24.82558206586144678, 1.605769216559448598 ) ) ;
#42202=CARTESIAN_POINT ( 'NONE',  ( -50.02370822792538974, -25.23256535379771037, 6.480020017899467355 ) ) ;
#42204=CARTESIAN_POINT ( 'NONE',  ( -8.236308187080631171, 18.58821751820538637, -1.500000000000002220 ) ) ;
#42205=VERTEX_POINT ( 'NONE', #84047 ) ;
#42206=CARTESIAN_POINT ( 'NONE',  ( -5.713817535623205046, 22.21719745612757535, 11.49999999999998934 ) ) ;
#42208=CARTESIAN_POINT ( 'NONE',  ( -127.5217000848324034, -23.96169478059714208, 10.65365249895716282 ) ) ;
#42209=ORIENTED_EDGE ( 'NONE', *, *, #28124, .T. ) ;
#42210=CARTESIAN_POINT ( 'NONE',  ( -49.13243839854418127, -25.28217150478232256, 4.246802725325826700 ) ) ;
#42212=B_SPLINE_CURVE_WITH_KNOTS ( 'NONE', 3,
 ( #88719, #41554, #34928, #81100 ),
 .UNSPECIFIED., .F., .F.,
 ( 4, 4 ),
 ( 0.000000000000000000, 0.0008333333333333525772 ),
 .UNSPECIFIED. ) ;
#42213=CARTESIAN_POINT ( 'NONE',  ( -30.47287095715008221, -23.78471427653590453, -0.9626557455456202783 ) ) ;
#42214=CARTESIAN_POINT ( 'NONE',  ( -1.756177585742932479, 21.11346882147791959, 11.49999999999999645 ) ) ;
#42215=CARTESIAN_POINT ( 'NONE',  ( -13.50798789833325664, 17.53495777034937220, -1.500000000000002220 ) ) ;
#42216=CARTESIAN_POINT ( 'NONE',  ( 10.54205562766345672, -17.70522803435136083, 11.49999999999998934 ) ) ;
#42217=ADVANCED_FACE ( 'NONE', ( #90662 ), #36878, .T. ) ;
#42219=CARTESIAN_POINT ( 'NONE',  ( -107.5228709571500758, -24.64898659630367916, 1.056161002820831474 ) ) ;
#42221=CARTESIAN_POINT ( 'NONE',  ( -54.59313660317440053, -24.15543982623906416, -0.2315651400026691176 ) ) ;
#42225=ORIENTED_EDGE ( 'NONE', *, *, #94312, .F. ) ;
#42227=CARTESIAN_POINT ( 'NONE',  ( -46.52287095715007581, -23.47593901973090524, -1.443836447538997314 ) ) ;
#42228=LINE ( 'NONE', #49837, #22803 ) ;
#42229=CARTESIAN_POINT ( 'NONE',  ( 20.64725891757762355, 2.036748910689437864, -1.500000000000002220 ) ) ;
#42230=CARTESIAN_POINT ( 'NONE',  ( -19.25911440464646063, 10.06369110047026538, 11.49999999999999645 ) ) ;
#42231=ORIENTED_EDGE ( 'NONE', *, *, #76044, .F. ) ;
#42232=B_SPLINE_CURVE_WITH_KNOTS ( 'NONE', 3,
 ( #75942, #83558, #7434, #29280 ),
 .UNSPECIFIED., .F., .F.,
 ( 4, 4 ),
 ( 1.387778780781445676E-17, 0.0001000000000000028508 ),
 .UNSPECIFIED. ) ;
#42233=ADVANCED_FACE ( 'NONE', ( #99748 ), #30251, .F. ) ;
#42235=CARTESIAN_POINT ( 'NONE',  ( -111.7814946224345789, -25.28710546256127145, 4.332404433089555695 ) ) ;
#42236=CARTESIAN_POINT ( 'NONE',  ( 19.55810785529653373, 10.91776788121007868, -1.500000000000002220 ) ) ;
#42237=EDGE_CURVE ( 'NONE', #92752, #503, #73381, .T. ) ;
#42238=ADVANCED_FACE ( 'NONE', ( #75924 ), #76917, .F. ) ;
#42243=FACE_OUTER_BOUND ( 'NONE', #22325, .T. ) ;
#42249=CARTESIAN_POINT ( 'NONE',  ( -69.62287095715005592, -23.73934037231756733, 11.05740245334329330 ) ) ;
#42250=EDGE_LOOP ( 'NONE', ( #10637, #6126, #80042, #44423 ) ) ;
#42251=CARTESIAN_POINT ( 'NONE',  ( 14.73992482348874411, 15.29747818672187165, -1.500000000000002220 ) ) ;
#42252=ORIENTED_EDGE ( 'NONE', *, *, #32587, .T. ) ;
#42253=CARTESIAN_POINT ( 'NONE',  ( -100.5774747013531822, -25.12365577940056482, 7.097838394941334172 ) ) ;
#42254=CARTESIAN_POINT ( 'NONE',  ( 3.337383349182757364, -21.60657791699550856, 11.49999999999998934 ) ) ;
#42255=DIRECTION ( 'NONE',  ( 0.000000000000000000, 0.9999999999976377785, 2.173523156925979975E-06 ) ) ;
#42258=CARTESIAN_POINT ( 'NONE',  ( 21.44370820036873937, 4.193779532373530294, -1.500000000000002220 ) ) ;
#42260=ORIENTED_EDGE ( 'NONE', *, *, #16319, .T. ) ;
#42263=EDGE_CURVE ( 'NONE', #86407, #89859, #25027, .T. ) ;
#42264=EDGE_CURVE ( 'NONE', #99862, #56477, #80754, .T. ) ;
#42265=VERTEX_POINT ( 'NONE', #40378 ) ;
#42266=CARTESIAN_POINT ( 'NONE',  ( -30.62525681927276011, -24.05323539164308855, 10.46343928437834414 ) ) ;
#42268=ORIENTED_EDGE ( 'NONE', *, *, #353, .T. ) ;
#42271=CARTESIAN_POINT ( 'NONE',  ( -30.61630412665073919, -24.37835529153250747, 0.3010598746230513933 ) ) ;
#42272=CARTESIAN_POINT ( 'NONE',  ( -15.93125441714207646, -14.09135727244061265, 11.49999999999998934 ) ) ;
#42273=DIRECTION ( 'NONE',  ( 1.000000000000000000, 3.773278334444167608E-23, 8.201307833595939069E-29 ) ) ;
#42275=ADVANCED_FACE ( 'NONE', ( #69322 ), #15525, .F. ) ;
#42276=CARTESIAN_POINT ( 'NONE',  ( -85.52211224428006631, -23.48783264082476308, -1.443836473390098796 ) ) ;
#42278=AXIS2_PLACEMENT_3D ( 'NONE', #41141, #93905, #80191 ) ;
#42279=CARTESIAN_POINT ( 'NONE',  ( -16.98888496755095545, 9.415225082695979353, -1.500000000000002220 ) ) ;
#42280=CARTESIAN_POINT ( 'NONE',  ( -117.5527607394227090, -24.51419770103158768, 9.386484678747166299 ) ) ;
#42282=CARTESIAN_POINT ( 'NONE',  ( -16.69004703121433408, -10.21020960635683394, 11.49999999999999645 ) ) ;
#42283=CARTESIAN_POINT ( 'NONE',  ( -81.62287095715008434, -23.47596703998600631, 11.44779298504227860 ) ) ;
#42284=CARTESIAN_POINT ( 'NONE',  ( -29.36005952620050863, -24.99996101429923812, 7.263710429510505939 ) ) ;
#42285=ORIENTED_EDGE ( 'NONE', *, *, #38290, .T. ) ;
#42286=EDGE_CURVE ( 'NONE', #63089, #89004, #93145, .T. ) ;
#42287=CARTESIAN_POINT ( 'NONE',  ( -117.5228709571500758, -23.95044443724993144, 10.65354141964648882 ) ) ;
#42288=CARTESIAN_POINT ( 'NONE',  ( -47.52287095715007581, -23.47593901973090169, -1.443836447538997092 ) ) ;
#42289=CARTESIAN_POINT ( 'NONE',  ( -90.52287095715004739, -24.52232992886363405, 0.6492154411906000400 ) ) ;
#42291=CARTESIAN_POINT ( 'NONE',  ( -88.62287095715004170, -23.48783264082479150, -1.443836473390063935 ) ) ;
#42292=CARTESIAN_POINT ( 'NONE',  ( 18.75866648459458830, -6.009157199652424453, 11.49999999999998934 ) ) ;
#42293=EDGE_CURVE ( 'NONE', #79556, #62504, #5616, .T. ) ;
#42295=CARTESIAN_POINT ( 'NONE',  ( -94.62287095715002749, -23.94994826722566117, -0.6494450866342748041 ) ) ;
#42298=VERTEX_POINT ( 'NONE', #31255 ) ;
#42301=CARTESIAN_POINT ( 'NONE',  ( -69.62287095715004170, -24.33832256526968862, 0.1851278514119857332 ) ) ;
#42303=CARTESIAN_POINT ( 'NONE',  ( -81.90695487689731635, -25.03722721891040948, 7.590183713343859218 ) ) ;
#42305=CARTESIAN_POINT ( 'NONE',  ( -79.52287095715004739, -23.48783264082476663, -1.443836473390090358 ) ) ;
#42306=CARTESIAN_POINT ( 'NONE',  ( 19.92730240972663935, 0.8534881809820089593, -1.500000000000002220 ) ) ;
#42307=CARTESIAN_POINT ( 'NONE',  ( -0.08206578796906692508, -21.98759388411814086, 10.03296377820838892 ) ) ;
#42308=CARTESIAN_POINT ( 'NONE',  ( -13.97081141688431138, 14.13901428111770819, -1.500000000000002220 ) ) ;
#42310=CARTESIAN_POINT ( 'NONE',  ( -71.52287095715007581, -24.33832256527048798, 0.1851278514138584019 ) ) ;
#42311=CARTESIAN_POINT ( 'NONE',  ( -29.52287095715004739, -23.65317350716957279, 11.05752279813568251 ) ) ;
#42312=CARTESIAN_POINT ( 'NONE',  ( -80.62364780861474856, -25.00182538069147142, 7.747789668545041586 ) ) ;
#42313=CARTESIAN_POINT ( 'NONE',  ( 6.705275102110877405, 19.67741782454948662, 11.49999999999999645 ) ) ;
#42314=CARTESIAN_POINT ( 'NONE',  ( -36.22287095715005734, -23.47593901973090169, -1.443836447538998202 ) ) ;
#42317=CARTESIAN_POINT ( 'NONE',  ( -0.7673284989158746239, 22.82873350090251918, 11.49999999999999645 ) ) ;
#42318=ORIENTED_EDGE ( 'NONE', *, *, #88664, .T. ) ;
#42320=CARTESIAN_POINT ( 'NONE',  ( -38.52287095715006870, -23.73907113217726916, -1.053371485780264294 ) ) ;
#42322=CARTESIAN_POINT ( 'NONE',  ( 12.36038202409810438, -16.04522380935875248, 11.49999999999998934 ) ) ;
#42326=EDGE_LOOP ( 'NONE', ( #61706, #18805, #72674, #93633 ) ) ;
#42328=CARTESIAN_POINT ( 'NONE',  ( -51.62287095715004881, -23.73907113216990084, -1.053371485793233475 ) ) ;
#42330=CARTESIAN_POINT ( 'NONE',  ( 17.67427751897593069, 9.450557017276361549, -1.500000000000002220 ) ) ;
#42331=CARTESIAN_POINT ( 'NONE',  ( -19.96636262075925927, 6.592627302904066511, 11.49999999999999645 ) ) ;
#42333=CARTESIAN_POINT ( 'NONE',  ( -124.6228709571500559, -24.64965695001469115, 8.947790433994175174 ) ) ;
#42334=CARTESIAN_POINT ( 'NONE',  ( 21.95769793831392036, 2.030053023538682222, 11.49999999999998934 ) ) ;
#42337=CARTESIAN_POINT ( 'NONE',  ( -81.88534077628074215, -29.50249666744127808, 6.293933732382250845 ) ) ;
#42339=CARTESIAN_POINT ( 'NONE',  ( -72.62362975610302840, -24.65952944569304250, 1.056160979905695463 ) ) ;
#42340=CARTESIAN_POINT ( 'NONE',  ( -31.50374477195024170, -23.96119346886880663, -0.6495511937832003646 ) ) ;
#42341=ADVANCED_FACE ( 'NONE', ( #47492 ), #29731, .T. ) ;
#42342=ORIENTED_EDGE ( 'NONE', *, *, #51036, .T. ) ;
#42347=DIRECTION ( 'NONE',  ( -3.773278334453080206E-23, 0.9999999999976377785, 2.173523156925979975E-06 ) ) ;
#42348=CARTESIAN_POINT ( 'NONE',  ( -13.21525772315781388, 15.71049578022273785, -1.500000000000002220 ) ) ;
#42353=CARTESIAN_POINT ( 'NONE',  ( -83.52287095715004739, -23.96127896941631619, -0.6493128931038049112 ) ) ;
#42354=CARTESIAN_POINT ( 'NONE',  ( 18.98964132805693694, -11.70494588174365092, -1.500000000000002220 ) ) ;
#42355=EDGE_CURVE ( 'NONE', #48556, #27910, #38325, .T. ) ;
#42356=ADVANCED_FACE ( 'NONE', ( #81443 ), #57617, .T. ) ;
#42357=B_SPLINE_CURVE_WITH_KNOTS ( 'NONE', 3,
 ( #3709, #58006, #88938, #19415, #15172, #13288, #85188, #77063 ),
 .UNSPECIFIED., .F., .F.,
 ( 4, 2, 2, 4 ),
 ( 6.384118678608834355E-06, 0.002007151183507251049, 0.003007534715921573835, 0.004007918248335896189 ),
 .UNSPECIFIED. ) ;
#42358=CARTESIAN_POINT ( 'NONE',  ( -47.52287095715004739, -24.66019654487199375, 8.947790411086122830 ) ) ;
#42360=ORIENTED_EDGE ( 'NONE', *, *, #15121, .F. ) ;
#42362=CARTESIAN_POINT ( 'NONE',  ( -47.92287095715007439, -23.47596703998600276, 11.44779298504227683 ) ) ;
#42363=CARTESIAN_POINT ( 'NONE',  ( -20.60679684081203789, -3.318877370925724879, 11.49999999999998934 ) ) ;
#42365=CARTESIAN_POINT ( 'NONE',  ( -39.04303308397305727, -25.28006866179717349, 4.215216948383927686 ) ) ;
#42366=ORIENTED_EDGE ( 'NONE', *, *, #19334, .T. ) ;
#42367=VERTEX_POINT ( 'NONE', #72336 ) ;
#42369=CARTESIAN_POINT ( 'NONE',  ( 9.758084087097168791, -18.66043984184860349, -1.500000000000002220 ) ) ;
#42371=CARTESIAN_POINT ( 'NONE',  ( -114.6228709571500701, -23.48783264082478794, -1.443836473390060382 ) ) ;
#42373=CARTESIAN_POINT ( 'NONE',  ( -120.6267747408976874, -24.15602025860899360, 10.28564288303534902 ) ) ;
#42374=CARTESIAN_POINT ( 'NONE',  ( -68.62287095715005592, -23.48786465467241058, 11.44779295918254647 ) ) ;
#42375=B_SPLINE_CURVE_WITH_KNOTS ( 'NONE', 3,
 ( #45713, #7138, #38088, #69042 ),
 .UNSPECIFIED., .F., .F.,
 ( 4, 4 ),
 ( 0.000000000000000000, 0.0004038461538461851630 ),
 .UNSPECIFIED. ) ;
#42377=CARTESIAN_POINT ( 'NONE',  ( 13.45394552336293614, 17.01807010946250287, -1.500000000000002220 ) ) ;
#42378=FACE_OUTER_BOUND ( 'NONE', #26133, .T. ) ;
#42379=CARTESIAN_POINT ( 'NONE',  ( -21.97457344801873447, 3.670769625195870134, 11.49999999999999645 ) ) ;
#42380=ORIENTED_EDGE ( 'NONE', *, *, #79298, .T. ) ;
#42381=DIRECTION ( 'NONE',  ( -3.773278334453079618E-23, 0.9999999999976377785, 2.173523156925979975E-06 ) ) ;
#42382=CARTESIAN_POINT ( 'NONE',  ( -95.55620429048339304, -23.48786465467241058, 11.44779295918254114 ) ) ;
#42384=CARTESIAN_POINT ( 'NONE',  ( -71.11462141275075055, -25.28903507783076776, 5.642180431236864635 ) ) ;
#42386=CARTESIAN_POINT ( 'NONE',  ( -40.62287095715004881, -24.83602698348161653, 1.605859176311265735 ) ) ;
#42387=ORIENTED_EDGE ( 'NONE', *, *, #23354, .T. ) ;
#42388=ADVANCED_FACE ( 'NONE', ( #89550 ), #13498, .T. ) ;
#42389=ORIENTED_EDGE ( 'NONE', *, *, #24050, .T. ) ;
#42391=VECTOR ( 'NONE', #62246, 1000.000000000000114 ) ;
#42392=CARTESIAN_POINT ( 'NONE',  ( -88.62287095715004170, -23.95044443724992078, 10.65354141964649237 ) ) ;
#42394=CARTESIAN_POINT ( 'NONE',  ( -51.52287095715006870, -24.64965694238407323, 8.947790433994203596 ) ) ;
#42395=ORIENTED_EDGE ( 'NONE', *, *, #90543, .F. ) ;
#42396=CARTESIAN_POINT ( 'NONE',  ( -130.5728709571500588, -24.69152398889280420, 9.136518679570812651 ) ) ;
#42397=CARTESIAN_POINT ( 'NONE',  ( -5.254942042970298210, 21.81482460008805546, -1.500000000000002220 ) ) ;
#42398=ORIENTED_EDGE ( 'NONE', *, *, #1504, .T. ) ;
#42399=CARTESIAN_POINT ( 'NONE',  ( -66.62287095715005592, -23.48783264082478439, -1.443836473390067487 ) ) ;
#42403=CARTESIAN_POINT ( 'NONE',  ( -30.59801660219940800, -24.66459861931856423, 1.095224832288508754 ) ) ;
#42405=VECTOR ( 'NONE', #17930, 1000.000000000000114 ) ;
#42406=CARTESIAN_POINT ( 'NONE',  ( -5.058734511472819051, -18.94576116945722788, 11.49999999999998934 ) ) ;
#42407=CARTESIAN_POINT ( 'NONE',  ( -46.56868028461229159, -23.48783264082476663, -1.443836473390096575 ) ) ;
#42409=ORIENTED_EDGE ( 'NONE', *, *, #93759, .T. ) ;
#42410=CARTESIAN_POINT ( 'NONE',  ( 11.68953838083566588, 18.09531432177502808, 11.49999999999998934 ) ) ;
#42412=CARTESIAN_POINT ( 'NONE',  ( -128.5894279438219883, -24.65952944569304961, 1.056160979905706787 ) ) ;
#42413=CARTESIAN_POINT ( 'NONE',  ( -80.88693734264360558, -25.30394771627923234, 5.024145871088269821 ) ) ;
#42414=CARTESIAN_POINT ( 'NONE',  ( -100.5995565470576167, -25.12159859110350979, 2.838444796902710010 ) ) ;
#42415=EDGE_CURVE ( 'NONE', #16063, #56862, #3827, .T. ) ;
#42416=PLANE ( 'NONE',  #18040 ) ;
#42417=CARTESIAN_POINT ( 'NONE',  ( 5.527175565732886042, -22.34193536506064603, -1.500000000000002220 ) ) ;
#42419=CARTESIAN_POINT ( 'NONE',  ( -47.52287095715006160, -24.65952944569304606, 1.056160979905693686 ) ) ;
#42421=CARTESIAN_POINT ( 'NONE',  ( 19.93115673323400117, -2.579441489355707606, 11.49999999999999645 ) ) ;
#42422=CARTESIAN_POINT ( 'NONE',  ( -68.58953762381672448, -23.47596703998600276, 11.44779298504227505 ) ) ;
#42423=CARTESIAN_POINT ( 'NONE',  ( -118.9228709571500531, -23.47593901973090524, -1.443836447538996426 ) ) ;
#42424=FACE_OUTER_BOUND ( 'NONE', #35867, .T. ) ;
#42425=DIRECTION ( 'NONE',  ( 0.000000000000000000, 2.173523156925980399E-06, -0.9999999999976378895 ) ) ;
#42427=CARTESIAN_POINT ( 'NONE',  ( -2.735935421901279696, -19.66989661884619522, 11.49999999999998934 ) ) ;
#42429=CARTESIAN_POINT ( 'NONE',  ( -18.24397684793207830, 7.494555614300850266, -1.500000000000002220 ) ) ;
#42430=CARTESIAN_POINT ( 'NONE',  ( -42.60032721050791338, -23.96119346886880663, -0.6495511937831991434 ) ) ;
#42433=CARTESIAN_POINT ( 'NONE',  ( 19.36870410414886479, 7.000668502413378569, 11.49999999999999645 ) ) ;
#42434=CARTESIAN_POINT ( 'NONE',  ( -115.6228709571500559, -24.99156045073393173, 7.747789690856161648 ) ) ;
#42435=CARTESIAN_POINT ( 'NONE',  ( -7.973561950239375307, 21.24132968703115765, 11.49999999999999645 ) ) ;
#42438=CARTESIAN_POINT ( 'NONE',  ( -69.78016143783460734, -25.12219113079085631, 6.955938379833897400 ) ) ;
#42439=CARTESIAN_POINT ( 'NONE',  ( -97.55489528667699517, -23.96119346886881374, -0.6495511937832056937 ) ) ;
#42441=PLANE ( 'NONE',  #38273 ) ;
#42442=B_SPLINE_CURVE_WITH_KNOTS ( 'NONE', 3,
 ( #14446, #92567, #23042, #54033 ),
 .UNSPECIFIED., .F., .F.,
 ( 4, 4 ),
 ( 0.2189169346825021734, 0.2199176817232675885 ),
 .UNSPECIFIED. ) ;
#42445=CARTESIAN_POINT ( 'NONE',  ( -99.47014701030484218, -25.19118371826951019, 6.667201686812183503 ) ) ;
#42446=CARTESIAN_POINT ( 'NONE',  ( -22.87863416751641310, 0.2071024363326711970, -1.500000000000002220 ) ) ;
#42447=CARTESIAN_POINT ( 'NONE',  ( -74.49974610374124495, -24.51314013834315375, 0.6176544820404125113 ) ) ;
#42449=CARTESIAN_POINT ( 'NONE',  ( -65.52287095715009002, -24.92579138211020151, 1.929029949965666235 ) ) ;
#42450=CARTESIAN_POINT ( 'NONE',  ( -14.39138815452349718, -17.32352244779961481, 11.49999999999999645 ) ) ;
#42451=VERTEX_POINT ( 'NONE', #65245 ) ;
#42454=CARTESIAN_POINT ( 'NONE',  ( -18.59763704738199408, -11.70098744416181979, -1.500000000000002220 ) ) ;
#42455=CARTESIAN_POINT ( 'NONE',  ( -111.5891439529568743, -24.34968618360933945, 0.1864209137778883862 ) ) ;
#42456=FACE_OUTER_BOUND ( 'NONE', #91942, .T. ) ;
#42458=ORIENTED_EDGE ( 'NONE', *, *, #60230, .F. ) ;
#42460=DIRECTION ( 'NONE',  ( 1.000000000000000000, 3.773278334444166432E-23, 8.201307841325785021E-29 ) ) ;
#42461=VERTEX_POINT ( 'NONE', #60613 ) ;
#42464=CARTESIAN_POINT ( 'NONE',  ( -17.09319154528168383, -11.34935287704045948, 11.49999999999998934 ) ) ;
#42466=ORIENTED_EDGE ( 'NONE', *, *, #99393, .F. ) ;
#42467=ORIENTED_EDGE ( 'NONE', *, *, #44345, .F. ) ;
#42469=CARTESIAN_POINT ( 'NONE',  ( 18.33865528945960577, 14.04639130150205872, 11.49999999999998934 ) ) ;
#42470=CARTESIAN_POINT ( 'NONE',  ( -104.5134480897169169, -24.35071581493544102, 9.817618358456019934 ) ) ;
#42471=CARTESIAN_POINT ( 'NONE',  ( -2.495337616714382367, -20.20711602426958819, -1.500000000000002220 ) ) ;
#42472=ADVANCED_FACE ( 'NONE', ( #67227 ), #6795, .F. ) ;
#42475=CARTESIAN_POINT ( 'NONE',  ( -51.69713094254252184, -25.26628317927419687, 3.905176899872079943 ) ) ;
#42478=CARTESIAN_POINT ( 'NONE',  ( -105.5090439743186721, -24.83618233451451118, 1.606449574219534826 ) ) ;
#42479=CARTESIAN_POINT ( 'NONE',  ( -71.31671495077925726, -25.25855297254991783, 7.173521560893385107 ) ) ;
#42481=CARTESIAN_POINT ( 'NONE',  ( -29.05456498926589504, -25.21531894358851389, 3.361079100850875356 ) ) ;
#42482=CARTESIAN_POINT ( 'NONE',  ( -86.52287095715006160, -23.48786465467241058, 11.44779295918254292 ) ) ;
#42485=ORIENTED_EDGE ( 'NONE', *, *, #90031, .F. ) ;
#42487=CARTESIAN_POINT ( 'NONE',  ( -0.3852054317258338245, -20.75737367715079174, -1.500000000000002220 ) ) ;
#42488=ORIENTED_EDGE ( 'NONE', *, *, #51871, .T. ) ;
#42489=CARTESIAN_POINT ( 'NONE',  ( -61.62287095715004881, -24.65952944569304606, 1.056160979905695907 ) ) ;
#42490=ORIENTED_EDGE ( 'NONE', *, *, #28408, .T. ) ;
#42491=LINE ( 'NONE', #10514, #58458 ) ;
#42492=CARTESIAN_POINT ( 'NONE',  ( -51.04357394935764347, -25.30543060587211812, 4.940877950953177056 ) ) ;
#42494=ORIENTED_EDGE ( 'NONE', *, *, #100264, .F. ) ;
#42495=CARTESIAN_POINT ( 'NONE',  ( -79.62287095715005592, -23.48783264082478794, -1.443836473390065489 ) ) ;
#42496=CARTESIAN_POINT ( 'NONE',  ( -116.6228709571500559, -23.73934037231757799, 11.05740245334328264 ) ) ;
#42497=CARTESIAN_POINT ( 'NONE',  ( -70.35895856474229504, -25.24515042133736387, 5.313173755051357361 ) ) ;
#42498=CARTESIAN_POINT ( 'NONE',  ( 20.41560922187292348, 8.460057656491983380, 11.49999999999999645 ) ) ;
#42500=CARTESIAN_POINT ( 'NONE',  ( -45.62287095715005592, -23.48786465467240703, 11.44779295918255002 ) ) ;
#42501=CARTESIAN_POINT ( 'NONE',  ( 18.14931799402153345, 13.46472642042223633, 11.49999999999998934 ) ) ;
#42502=CARTESIAN_POINT ( 'NONE',  ( -46.52287095715004028, -24.35013146730202394, 9.818937971375106599 ) ) ;
#42503=ORIENTED_EDGE ( 'NONE', *, *, #18065, .F. ) ;
#42504=VERTEX_POINT ( 'NONE', #22007 ) ;
#42505=FACE_OUTER_BOUND ( 'NONE', #52679, .T. ) ;
#42508=ORIENTED_EDGE ( 'NONE', *, *, #68361, .T. ) ;
#42509=CARTESIAN_POINT ( 'NONE',  ( -21.05374637409849825, 2.266213160971460194, -1.500000000000002220 ) ) ;
#42510=CARTESIAN_POINT ( 'NONE',  ( -125.5228709571500616, -29.50250786944525672, 11.44777988621622633 ) ) ;
#42511=CARTESIAN_POINT ( 'NONE',  ( -40.66978929498593942, -25.29385509343200766, 5.536656401469072009 ) ) ;
#42512=CARTESIAN_POINT ( 'NONE',  ( 15.07672925556244969, 16.42598562245719407, -1.500000000000002220 ) ) ;
#42513=CARTESIAN_POINT ( 'NONE',  ( -50.04527796557857755, -25.03220900868303644, 7.536031501934568944 ) ) ;
#42517=CARTESIAN_POINT ( 'NONE',  ( -36.50466263922482568, -23.96169478059712432, 10.65365249895718591 ) ) ;
#42518=CARTESIAN_POINT ( 'NONE',  ( -83.58953762381672448, -24.64965694238407323, 8.947790433994653014 ) ) ;
#42519=B_SPLINE_CURVE_WITH_KNOTS ( 'NONE', 3,
 ( #79684, #73090, #4576, #66497 ),
 .UNSPECIFIED., .F., .F.,
 ( 4, 4 ),
 ( 0.000000000000000000, 9.999999999998897304E-05 ),
 .UNSPECIFIED. ) ;
#42520=CARTESIAN_POINT ( 'NONE',  ( 16.17817332762582794, -10.88531698672339942, -1.500000000000002220 ) ) ;
#42521=VECTOR ( 'NONE', #48392, 1000.000000000000114 ) ;
#42522=CARTESIAN_POINT ( 'NONE',  ( 17.68986881342592454, -12.14045624799103962, -1.500000000000002220 ) ) ;
#42525=CARTESIAN_POINT ( 'NONE',  ( -107.5228709571500758, -23.48786465467241769, 11.44779295918253936 ) ) ;
#42526=DIRECTION ( 'NONE',  ( 0.000000000000000000, -2.173523156925979552E-06, 0.9999999999976378895 ) ) ;
#42528=CARTESIAN_POINT ( 'NONE',  ( -19.63924127562733446, 11.44998032699685631, -1.500000000000002220 ) ) ;
#42529=EDGE_CURVE ( 'NONE', #79651, #26860, #71051, .T. ) ;
#42531=PLANE ( 'NONE',  #69325 ) ;
#42533=CARTESIAN_POINT ( 'NONE',  ( -15.73602684802347440, -12.20685706852216867, 11.49999999999999645 ) ) ;
#42534=CARTESIAN_POINT ( 'NONE',  ( -101.6228709571500559, -24.51387760970723662, 9.387446482453405849 ) ) ;
#42535=CARTESIAN_POINT ( 'NONE',  ( -128.5228709571501042, -23.72773821059536914, 11.05748984161097326 ) ) ;
#42536=CARTESIAN_POINT ( 'NONE',  ( -128.5228709571501042, -24.66019654487200441, 8.947790411086108620 ) ) ;
#42537=ORIENTED_EDGE ( 'NONE', *, *, #81323, .F. ) ;
#42538=DIRECTION ( 'NONE',  ( -0.000000000000000000, 2.173523156925979552E-06, -0.9999999999976378895 ) ) ;
#42539=CARTESIAN_POINT ( 'NONE',  ( -33.01375014246017514, -24.87479601683088148, 8.247789944647561100 ) ) ;
#42540=CARTESIAN_POINT ( 'NONE',  ( 21.38347125639554136, -3.707035686939989638, -1.500000000000002220 ) ) ;
#42541=CARTESIAN_POINT ( 'NONE',  ( -50.79429371764780399, -25.04955745062598282, 7.532901908008377667 ) ) ;
#42542=CARTESIAN_POINT ( 'NONE',  ( 8.254404603115069960, -17.72612730319335839, -1.500000000000002220 ) ) ;
#42543=CARTESIAN_POINT ( 'NONE',  ( -100.6228709571500559, -25.00182538069145721, 7.747789668545099317 ) ) ;
#42544=VECTOR ( 'NONE', #94151, 1000.000000000000114 ) ;
#42547=CARTESIAN_POINT ( 'NONE',  ( -60.62287095715005592, -24.92604778743016780, 8.074972756849359001 ) ) ;
#42548=CARTESIAN_POINT ( 'NONE',  ( -19.82921842031888104, 5.099586017421429140, 11.49999999999999645 ) ) ;
#42552=CARTESIAN_POINT ( 'NONE',  ( -114.6228709571500701, -23.47596703998600631, 11.44779298504227860 ) ) ;
#42556=LINE ( 'NONE', #89215, #36391 ) ;
#42557=DIRECTION ( 'NONE',  ( 0.000000000000000000, -0.9999999999976377785, -2.173523156925979128E-06 ) ) ;
#42558=AXIS2_PLACEMENT_3D ( 'NONE', #49613, #47605, #80041 ) ;
#42559=CARTESIAN_POINT ( 'NONE',  ( -109.5865577389930650, -24.65952944569305316, 1.056160979905708786 ) ) ;
#42560=ORIENTED_EDGE ( 'NONE', *, *, #76468, .T. ) ;
#42561=DIRECTION ( 'NONE',  ( -3.773278334444166432E-23, 1.000000000000000000, 0.000000000000000000 ) ) ;
#42562=CARTESIAN_POINT ( 'NONE',  ( 18.48385363477634513, -13.70420857335572506, 11.49999999999999645 ) ) ;
#42563=CARTESIAN_POINT ( 'NONE',  ( -9.471985145535571249, 20.67137392225973258, 11.49999999999998934 ) ) ;
#42564=CARTESIAN_POINT ( 'NONE',  ( -110.5141131277583639, -24.52399227489124556, 9.353111116836533512 ) ) ;
#42565=B_SPLINE_SURFACE_WITH_KNOTS ( 'NONE', 3, 3, ( 
 ( #19503, #95638, #71809, #33231 ),
 ( #79901, #95136, #19002, #79402 ),
 ( #26123, #49479, #49982, #25110 ),
 ( #48971, #80908, #57094, #27126 ),
 ( #41352, #80409, #11399, #72306 ),
 ( #58092, #10902, #11893, #94630 ),
 ( #41866, #89027, #4291, #2802 ),
 ( #42373, #42863, #3313, #73306 ),
 ( #73792, #56086, #74295, #89519 ),
 ( #60585, #35241, #28125, #28619 ) ),
 .UNSPECIFIED., .F., .F., .F.,
 ( 4, 3, 3, 4 ),
 ( 4, 4 ),
 ( 0.7022005934544809369, 0.7765311282028795059, 0.8508616629512781859, 0.9995227324480755460 ),
 ( 0.09950600549362356717, 0.1005780349481100455 ),
 .UNSPECIFIED. ) ;
#42566=CARTESIAN_POINT ( 'NONE',  ( -122.5228709571500616, -24.64898659630368272, 1.056161002820833028 ) ) ;
#42567=CARTESIAN_POINT ( 'NONE',  ( -50.52287095715006160, -25.00158670708909270, 2.256160236439166411 ) ) ;
#42568=CARTESIAN_POINT ( 'NONE',  ( -69.34303308397305443, -25.25559839591755207, 6.209207386190695566 ) ) ;
#42569=CARTESIAN_POINT ( 'NONE',  ( -15.13543854793762300, 15.80457324685279374, -1.500000000000002220 ) ) ;
#42572=CARTESIAN_POINT ( 'NONE',  ( -120.5228709571500900, -25.00182538069145366, 7.747789668545101982 ) ) ;
#42577=CARTESIAN_POINT ( 'NONE',  ( -20.22731604866883970, -2.807383831903240257, -1.500000000000002220 ) ) ;
#42579=ORIENTED_EDGE ( 'NONE', *, *, #25403, .F. ) ;
#42580=VERTEX_POINT ( 'NONE', #78175 ) ;
#42582=CARTESIAN_POINT ( 'NONE',  ( 0.2859537766682072601, -23.01552763051285666, 11.49999999999998934 ) ) ;
#42583=DIRECTION ( 'NONE',  ( 0.000000000000000000, 0.9999999999976377785, 2.173523156925979128E-06 ) ) ;
#42584=CARTESIAN_POINT ( 'NONE',  ( -16.67386609800740516, 11.36076560755915033, -1.500000000000002220 ) ) ;
#42585=ORIENTED_EDGE ( 'NONE', *, *, #68687, .T. ) ;
#42586=DIRECTION ( 'NONE',  ( 1.000000000000000000, 3.773278334444167608E-23, 8.201307833595939069E-29 ) ) ;
#42587=CARTESIAN_POINT ( 'NONE',  ( -77.62287095715009855, -23.47596703998600631, 11.44779298504227683 ) ) ;
#42588=CARTESIAN_POINT ( 'NONE',  ( -95.50150878202170190, -25.00158670708911046, 2.256160236439221034 ) ) ;
#42589=CARTESIAN_POINT ( 'NONE',  ( -108.6228709571500559, -29.50248528299804818, 1.056150453629043584 ) ) ;
#42590=CARTESIAN_POINT ( 'NONE',  ( 15.12546962493697933, 15.13007008128210096, 11.49999999999999645 ) ) ;
#42592=CARTESIAN_POINT ( 'NONE',  ( -55.52287095715006870, -24.91544648472619983, 1.928969306349232360 ) ) ;
#42593=VECTOR ( 'NONE', #93423, 1000.000000000000114 ) ;
#42594=EDGE_CURVE ( 'NONE', #17644, #29613, #97635, .T. ) ;
#42595=ORIENTED_EDGE ( 'NONE', *, *, #79921, .T. ) ;
#42596=CARTESIAN_POINT ( 'NONE',  ( 0.6114060112162268412, -22.25658958135186793, 11.49999999999998934 ) ) ;
#42597=EDGE_CURVE ( 'NONE', #77757, #28152, #62606, .T. ) ;
#42598=CARTESIAN_POINT ( 'NONE',  ( -14.21563987850626276, 15.01860006206015008, -1.500000000000002220 ) ) ;
#42600=CARTESIAN_POINT ( 'NONE',  ( -71.73006576507869170, -25.03707830618030172, 7.590867772707287742 ) ) ;
#42601=EDGE_LOOP ( 'NONE', ( #40954, #63428, #25304, #33000 ) ) ;
#42602=CARTESIAN_POINT ( 'NONE',  ( -56.52287095715006160, -24.33832256527049154, 0.1851278514138608444 ) ) ;
#42603=EDGE_LOOP ( 'NONE', ( #50611, #72913, #50947, #9011 ) ) ;
#42605=CARTESIAN_POINT ( 'NONE',  ( -11.48448384864204996, -17.54081393385053644, -1.500000000000002220 ) ) ;
#42607=CARTESIAN_POINT ( 'NONE',  ( 21.74639208212181529, -2.611101805624240768, 11.49999999999999645 ) ) ;
#42608=CARTESIAN_POINT ( 'NONE',  ( -73.54545617769827004, -24.35071581493543036, 9.817618358456027039 ) ) ;
#42609=CARTESIAN_POINT ( 'NONE',  ( 5.070899574700155732, -21.93562493352797915, 11.49999999999998934 ) ) ;
#42610=CARTESIAN_POINT ( 'NONE',  ( -8.544475976622297964, 19.10969517993760292, 11.49999999999998934 ) ) ;
#42611=CARTESIAN_POINT ( 'NONE',  ( -110.5228709571500616, -24.99132157543167310, 2.256160258750667502 ) ) ;
#42613=CARTESIAN_POINT ( 'NONE',  ( -29.62287095715005236, -23.66089804901488947, 11.05752276264044021 ) ) ;
#42615=ORIENTED_EDGE ( 'NONE', *, *, #9351, .T. ) ;
#42616=CARTESIAN_POINT ( 'NONE',  ( -84.55620429048339304, -23.48786465467241413, 11.44779295918254469 ) ) ;
#42619=DIRECTION ( 'NONE',  ( -3.773278334453079618E-23, 0.9999999999976377785, 2.173523156925979975E-06 ) ) ;
#42620=ORIENTED_EDGE ( 'NONE', *, *, #74125, .F. ) ;
#42621=CARTESIAN_POINT ( 'NONE',  ( 21.36505145794347982, 1.902718533054148509, -1.500000000000002220 ) ) ;
#42624=CARTESIAN_POINT ( 'NONE',  ( 15.50021099394596646, 14.30638080151107694, 11.49999999999998934 ) ) ;
#42625=CARTESIAN_POINT ( 'NONE',  ( -99.53456258256274225, -25.26500153315007324, 3.892973016135182096 ) ) ;
#42627=CARTESIAN_POINT ( 'NONE',  ( -50.57159555137985052, -23.48786465467240347, 11.44779295918255002 ) ) ;
#42628=CARTESIAN_POINT ( 'NONE',  ( -101.6314100629513035, -23.96119346886880663, -0.6495511937832048055 ) ) ;
#42629=CARTESIAN_POINT ( 'NONE',  ( -129.5560488321862351, -23.73791477778912551, 11.05961554403170055 ) ) ;
#42630=CARTESIAN_POINT ( 'NONE',  ( 11.82310115920509830, 18.66461490495635545, -1.500000000000002220 ) ) ;
#42633=CARTESIAN_POINT ( 'NONE',  ( -81.50253896702017187, -24.51419770103159834, 9.386484678747182286 ) ) ;
#42634=B_SPLINE_CURVE_WITH_KNOTS ( 'NONE', 3,
 ( #36234, #29603, #82890, #53463 ),
 .UNSPECIFIED., .F., .F.,
 ( 4, 4 ),
 ( 0.07055037829823759821, 0.07955680957035315970 ),
 .UNSPECIFIED. ) ;
#42635=CARTESIAN_POINT ( 'NONE',  ( -113.6228709571500559, -29.50247984919015209, -1.443849546365048253 ) ) ;
#42636=CARTESIAN_POINT ( 'NONE',  ( -40.53889064818358889, -25.27956071218200762, 5.542732955578356879 ) ) ;
#42637=B_SPLINE_CURVE_WITH_KNOTS ( 'NONE', 3,
 ( #651, #7764, #92990, #22469, #92495, #93491 ),
 .UNSPECIFIED., .F., .F.,
 ( 4, 2, 4 ),
 ( 0.000000000000000000, 0.001380901958385388545, 0.002761803916770777089 ),
 .UNSPECIFIED. ) ;
#42638=B_SPLINE_CURVE_WITH_KNOTS ( 'NONE', 3,
 ( #68949, #30381, #99873, #29884 ),
 .UNSPECIFIED., .F., .F.,
 ( 4, 4 ),
 ( 0.000000000000000000, 9.999999999998897304E-05 ),
 .UNSPECIFIED. ) ;
#42639=ADVANCED_FACE ( 'NONE', ( #65003 ), #45966, .T. ) ;
#42640=CARTESIAN_POINT ( 'NONE',  ( -25.50502449915233072, -24.92980806509333647, 6.075536601959949934 ) ) ;
#42641=B_SPLINE_CURVE_WITH_KNOTS ( 'NONE', 3,
 ( #98897, #53747, #77055, #38508 ),
 .UNSPECIFIED., .F., .F.,
 ( 4, 4 ),
 ( 0.000000000000000000, 0.003057692307692316813 ),
 .UNSPECIFIED. ) ;
#42643=CARTESIAN_POINT ( 'NONE',  ( -11.21157863559261791, -18.18922556752850994, -1.500000000000002220 ) ) ;
#42644=CARTESIAN_POINT ( 'NONE',  ( -69.98187464599547525, -25.05189924121757272, 7.521888907215067199 ) ) ;
#42645=CARTESIAN_POINT ( 'NONE',  ( -79.62287095715005592, -29.50250786944525672, 11.44777988621623521 ) ) ;
#42646=EDGE_CURVE ( 'NONE', #48546, #64856, #51642, .T. ) ;
#42649=CARTESIAN_POINT ( 'NONE',  ( -22.56969522194696509, -0.6267768857631424995, -1.500000000000002220 ) ) ;
#42650=B_SPLINE_SURFACE_WITH_KNOTS ( 'NONE', 3, 3, ( 
 ( #30693, #32187, #85472, #45935 ),
 ( #76845, #61666, #38801, #15957 ),
 ( #92582, #61170, #37812, #84976 ),
 ( #15461, #78354, #69763, #243 ),
 ( #62160, #23567, #86478, #8354 ),
 ( #743, #24074, #94087, #55043 ),
 ( #85981, #8855, #1752, #17973 ) ),
 .UNSPECIFIED., .F., .F., .F.,
 ( 4, 3, 4 ),
 ( 4, 4 ),
 ( 0.0004766839783823611197, 0.1029713700210900251, 0.2054660560637976974 ),
 ( 0.05950913535538977089, 0.06054931731713387305 ),
 .UNSPECIFIED. ) ;
#42651=CARTESIAN_POINT ( 'NONE',  ( -70.62287095715005592, -29.50250786944525672, 11.44777988621623699 ) ) ;
#42652=EDGE_LOOP ( 'NONE', ( #30707, #78035, #46721, #78429 ) ) ;
#42653=DIRECTION ( 'NONE',  ( 0.000000000000000000, 0.9999999999976377785, 2.173523156925979975E-06 ) ) ;
#42654=DIRECTION ( 'NONE',  ( -3.773278334453079618E-23, 0.9999999999976377785, 2.173523156925979975E-06 ) ) ;
#42655=CARTESIAN_POINT ( 'NONE',  ( 12.99534586470982234, -14.87506298573330632, 11.49999999999999645 ) ) ;
#42656=CARTESIAN_POINT ( 'NONE',  ( -126.6228709571500559, -23.48786465467242124, 11.44779295918253403 ) ) ;
#42657=CARTESIAN_POINT ( 'NONE',  ( -67.63597519206453512, -24.15543982623906771, -0.2315651400026651485 ) ) ;
#42658=ORIENTED_EDGE ( 'NONE', *, *, #42153, .F. ) ;
#42660=CARTESIAN_POINT ( 'NONE',  ( -29.61081252053125112, -24.60094231151948208, 3.196431696360289010 ) ) ;
#42661=AXIS2_PLACEMENT_3D ( 'NONE', #7646, #61446, #67561 ) ;
#42663=CARTESIAN_POINT ( 'NONE',  ( -11.89702471719568244, -18.04982639819725776, 11.49999999999998934 ) ) ;
#42664=CARTESIAN_POINT ( 'NONE',  ( -76.52287095715007581, -24.64898659630528854, 1.056161002820826145 ) ) ;
#42665=CARTESIAN_POINT ( 'NONE',  ( -17.66094656686658482, 7.961706694365092041, -1.500000000000002220 ) ) ;
#42667=LINE ( 'NONE', #55498, #58833 ) ;
#42668=CARTESIAN_POINT ( 'NONE',  ( 1.028332004353105233, 19.75660188889424518, 11.49999999999998934 ) ) ;
#42671=CARTESIAN_POINT ( 'NONE',  ( 19.74221769882431587, -4.499994434135383692, 11.49999999999999645 ) ) ;
#42674=ORIENTED_EDGE ( 'NONE', *, *, #94194, .T. ) ;
#42675=CARTESIAN_POINT ( 'NONE',  ( -100.0625863431822324, -25.30020101379185959, 4.636546911730082599 ) ) ;
#42678=DIRECTION ( 'NONE',  ( 0.000000000000000000, 2.173523156925980399E-06, -0.9999999999976378895 ) ) ;
#42680=CARTESIAN_POINT ( 'NONE',  ( 11.63622169266987783, 16.31392799894670631, -1.500000000000002220 ) ) ;
#42682=ORIENTED_EDGE ( 'NONE', *, *, #47369, .F. ) ;
#42683=ADVANCED_FACE ( 'NONE', ( #67473 ), #6214, .T. ) ;
#42685=CARTESIAN_POINT ( 'NONE',  ( -50.27385278553439463, -25.26258884680880712, 4.732894951404434281 ) ) ;
#42687=CARTESIAN_POINT ( 'NONE',  ( -80.36267167646580845, -25.30553951917087119, 4.968573168359604608 ) ) ;
#42689=FACE_OUTER_BOUND ( 'NONE', #44205, .T. ) ;
#42690=CARTESIAN_POINT ( 'NONE',  ( -89.40841769935768468, -25.18330262420952437, 6.757888864229147252 ) ) ;
#42692=CARTESIAN_POINT ( 'NONE',  ( -116.6228709571500559, -24.65952944569305316, 1.056160979905706121 ) ) ;
#42694=CARTESIAN_POINT ( 'NONE',  ( -15.63206872509828571, 12.99414084278249071, -1.500000000000002220 ) ) ;
#42696=ORIENTED_EDGE ( 'NONE', *, *, #18083, .T. ) ;
#42697=EDGE_CURVE ( 'NONE', #67032, #54301, #32208, .T. ) ;
#42698=CARTESIAN_POINT ( 'NONE',  ( -22.60589916338503613, 3.847557683979087706, -1.500000000000002220 ) ) ;
#42699=CARTESIAN_POINT ( 'NONE',  ( -32.65885280296615178, -23.73766607897670866, -1.055555164236442023 ) ) ;
#42704=CARTESIAN_POINT ( 'NONE',  ( 7.804836024166685426, 19.70032748343534834, 11.49999999999999645 ) ) ;
#42705=EDGE_CURVE ( 'NONE', #82541, #21005, #35531, .T. ) ;
#42706=CARTESIAN_POINT ( 'NONE',  ( -22.11188964843745453, -1.696007508606716341, -1.500000000000002220 ) ) ;
#42707=EDGE_CURVE ( 'NONE', #14471, #29214, #75062, .T. ) ;
#42708=CARTESIAN_POINT ( 'NONE',  ( 6.154377932377651739, 19.64630176443789367, 11.49999999999998934 ) ) ;
#42710=CARTESIAN_POINT ( 'NONE',  ( -41.58699204436209129, -24.34968618360933590, 0.1864209137778856940 ) ) ;
#42711=ORIENTED_EDGE ( 'NONE', *, *, #15306, .T. ) ;
#42713=LINE ( 'NONE', #97478, #95623 ) ;
#42716=APPLICATION_CONTEXT ( 'configuration controlled 3d designs of mechanical parts and assemblies' ) ;
#42718=CARTESIAN_POINT ( 'NONE',  ( -59.62287095715004881, -29.50250243563736774, 8.947779886222145151 ) ) ;
#42719=CARTESIAN_POINT ( 'NONE',  ( -28.55247368671063768, -23.80130948982615280, 10.65365253163527193 ) ) ;
#42721=CARTESIAN_POINT ( 'NONE',  ( 8.056674255711671506, 19.11000797562349618, -1.500000000000002220 ) ) ;
#42722=ADVANCED_FACE ( 'NONE', ( #13164 ), #89310, .F. ) ;
#42723=CARTESIAN_POINT ( 'NONE',  ( -21.53672441135761773, -2.854535511010750870, 11.49999999999999645 ) ) ;
#42727=CARTESIAN_POINT ( 'NONE',  ( -115.5510445847871779, -24.83618233451450408, 1.606449574219536824 ) ) ;
#42728=CARTESIAN_POINT ( 'NONE',  ( -21.57557905285345612, -6.117077608415351087, -1.500000000000002220 ) ) ;
#42733=CARTESIAN_POINT ( 'NONE',  ( -89.54303308397305727, -25.05712135967894838, 7.447789548357303779 ) ) ;
#42736=EDGE_LOOP ( 'NONE', ( #83687, #6424, #86870, #14968 ) ) ;
#42737=DIRECTION ( 'NONE',  ( -3.773278334453079030E-23, 0.9999999999976377785, 2.173523156925979128E-06 ) ) ;
#42739=CARTESIAN_POINT ( 'NONE',  ( -16.85803360905838488, 12.98640638483674259, -1.500000000000002220 ) ) ;
#42740=ORIENTED_EDGE ( 'NONE', *, *, #4649, .T. ) ;
#42741=CARTESIAN_POINT ( 'NONE',  ( -68.62287095715008434, -24.34917612406838217, 0.1852690917426622341 ) ) ;
#42742=CARTESIAN_POINT ( 'NONE',  ( 16.27406392464308027, 14.57352745747340172, 11.49999999999998934 ) ) ;
#42743=DIRECTION ( 'NONE',  ( 0.000000000000000000, -0.9999999999976377785, -2.173523156925979128E-06 ) ) ;
#42744=CARTESIAN_POINT ( 'NONE',  ( -5.639450322166912777, -21.95568564230989850, 11.49999999999998934 ) ) ;
#42746=LINE ( 'NONE', #35123, #7662 ) ;
#42747=CARTESIAN_POINT ( 'NONE',  ( -11.13288495942205536, 18.84158392345546318, -1.500000000000002220 ) ) ;
#42750=LINE ( 'NONE', #73683, #59919 ) ;
#42751=CARTESIAN_POINT ( 'NONE',  ( -75.52287095715006160, -24.99156044556120548, 7.747789690856173195 ) ) ;
#42752=ORIENTED_EDGE ( 'NONE', *, *, #73559, .T. ) ;
#42755=CARTESIAN_POINT ( 'NONE',  ( -44.52287095715006160, -24.65952944569303895, 1.056160979905691910 ) ) ;
#42756=CARTESIAN_POINT ( 'NONE',  ( -10.20961666403812096, -23.56687617480621455, 2.712351064733613537 ) ) ;
#42757=CARTESIAN_POINT ( 'NONE',  ( 14.70648301983428397, -15.34743991077593250, -1.500000000000002220 ) ) ;
#42759=CARTESIAN_POINT ( 'NONE',  ( -26.48766330312332684, -24.75186131672143475, 3.017960868138962027 ) ) ;
#42760=CARTESIAN_POINT ( 'NONE',  ( -85.65008181500884632, -23.48783264082476308, -1.443836473390099018 ) ) ;
#42761=CARTESIAN_POINT ( 'NONE',  ( -68.50127936046202137, -24.34968618360933590, 0.1864209137778813363 ) ) ;
#42764=CARTESIAN_POINT ( 'NONE',  ( -44.62287095715004881, -24.64965695001468404, 8.947790433994187609 ) ) ;
#42765=VERTEX_POINT ( 'NONE', #73588 ) ;
#42766=CARTESIAN_POINT ( 'NONE',  ( -16.13938233076020268, 11.07636124087057183, 11.49999999999999645 ) ) ;
#42767=CARTESIAN_POINT ( 'NONE',  ( -95.62287095715005592, -23.48783264082479150, -1.443836473390061936 ) ) ;
#42768=AXIS2_PLACEMENT_3D ( 'NONE', #36773, #97174, #75817 ) ;
#42769=B_SPLINE_CURVE_WITH_KNOTS ( 'NONE', 3,
 ( #68124, #99045, #29545, #60522 ),
 .UNSPECIFIED., .F., .F.,
 ( 4, 4 ),
 ( 0.000000000000000000, 0.0001000000000000028644 ),
 .UNSPECIFIED. ) ;
#42770=CARTESIAN_POINT ( 'NONE',  ( -29.76915174891760429, -25.21382154147696042, 5.865244179202782959 ) ) ;
#42773=CARTESIAN_POINT ( 'NONE',  ( -99.74640623490535063, -25.31439576479845144, 5.397458638819514931 ) ) ;
#42775=CARTESIAN_POINT ( 'NONE',  ( -81.01753736565918018, -25.03156042079280397, 7.476685952954507997 ) ) ;
#42776=CARTESIAN_POINT ( 'NONE',  ( -13.08164486973500118, 14.69858247433046650, -1.500000000000002220 ) ) ;
#42777=ORIENTED_EDGE ( 'NONE', *, *, #3278, .F. ) ;
#42778=CARTESIAN_POINT ( 'NONE',  ( -91.62287095715004170, -29.50250243563736774, 8.947779886222139822 ) ) ;
#42780=EDGE_CURVE ( 'NONE', #80623, #47537, #44460, .T. ) ;
#42782=ORIENTED_EDGE ( 'NONE', *, *, #19817, .T. ) ;
#42783=LINE ( 'NONE', #67122, #19195 ) ;
#42784=LINE ( 'NONE', #2222, #40990 ) ;
#42785=CARTESIAN_POINT ( 'NONE',  ( -55.66784212058755799, -23.48783264082475952, -1.443836473390099462 ) ) ;
#42787=CARTESIAN_POINT ( 'NONE',  ( -80.91269838580346629, -25.14083923594767356, 2.947789366383930965 ) ) ;
#42788=EDGE_CURVE ( 'NONE', #50770, #14217, #33478, .T. ) ;
#42789=CARTESIAN_POINT ( 'NONE',  ( -69.34303308397305443, -25.31201785239418811, 6.209207263561717483 ) ) ;
#42790=CARTESIAN_POINT ( 'NONE',  ( -79.52287095715006160, -24.65952944569304961, 1.056160979905698794 ) ) ;
#42791=CARTESIAN_POINT ( 'NONE',  ( 13.74685606122050885, 14.44317598224977672, 11.49999999999998934 ) ) ;
#42793=CARTESIAN_POINT ( 'NONE',  ( -0.03481313173224404034, -22.59931665215008323, 1.725801405104978370 ) ) ;
#42794=CARTESIAN_POINT ( 'NONE',  ( 7.614665684681447111, -18.39110272641453037, -1.500000000000002220 ) ) ;
#42799=AXIS2_PLACEMENT_3D ( 'NONE', #87995, #89485, #50431 ) ;
#42805=CARTESIAN_POINT ( 'NONE',  ( -51.15959938089677195, -25.22513071276370766, 3.603215203315445869 ) ) ;
#42808=CARTESIAN_POINT ( 'NONE',  ( -127.5894462411159225, -24.51314013834317151, 0.6176544820404252789 ) ) ;
#42809=ORIENTED_EDGE ( 'NONE', *, *, #63272, .F. ) ;
#42810=CARTESIAN_POINT ( 'NONE',  ( 20.17645099164838030, 1.678240329834772115, 11.49999999999998934 ) ) ;
#42811=EDGE_CURVE ( 'NONE', #84010, #63074, #61357, .T. ) ;
#42813=B_SPLINE_CURVE_WITH_KNOTS ( 'NONE', 3,
 ( #62390, #93320, #54784, #49180 ),
 .UNSPECIFIED., .F., .F.,
 ( 4, 4 ),
 ( 0.5101502102554993368, 0.5191566415276147595 ),
 .UNSPECIFIED. ) ;
#42819=CARTESIAN_POINT ( 'NONE',  ( 7.608091486120485136, 18.53616061196756704, -1.500000000000002220 ) ) ;
#42820=CARTESIAN_POINT ( 'NONE',  ( 16.07406896385161943, -13.52096256729613266, 11.49999999999999645 ) ) ;
#42822=CARTESIAN_POINT ( 'NONE',  ( -70.58658433434442259, -24.63419186844611275, 9.035850630976918652 ) ) ;
#42823=CARTESIAN_POINT ( 'NONE',  ( -16.84257673422482426, -14.26466048179180568, 11.49999999999998934 ) ) ;
#42824=EDGE_CURVE ( 'NONE', #909, #100104, #23768, .T. ) ;
#42826=LINE ( 'NONE', #75248, #59775 ) ;
#42828=EDGE_CURVE ( 'NONE', #27734, #86526, #60100, .T. ) ;
#42829=CARTESIAN_POINT ( 'NONE',  ( -72.60739634760311390, -23.48783264082477018, -1.443836473390095021 ) ) ;
#42830=B_SPLINE_SURFACE_WITH_KNOTS ( 'NONE', 3, 3, ( 
 ( #82829, #7200, #30543, #44291 ),
 ( #14310, #67139, #75220, #45284 ),
 ( #76210, #37165, #53896, #13811 ),
 ( #45775, #67628, #98048, #6704 ),
 ( #13312, #76698, #38148, #44786 ),
 ( #60520, #46273, #59513, #5712 ),
 ( #98549, #37660, #29045, #68615 ) ),
 .UNSPECIFIED., .F., .F., .F.,
 ( 4, 3, 4 ),
 ( 4, 4 ),
 ( 0.0004766839783822517779, 0.1029713700210901639, 0.2054660560637980860 ),
 ( 0.1095218577375331737, 0.1105851154774898787 ),
 .UNSPECIFIED. ) ;
#42831=FACE_OUTER_BOUND ( 'NONE', #93337, .T. ) ;
#42832=ORIENTED_EDGE ( 'NONE', *, *, #56912, .T. ) ;
#42833=EDGE_LOOP ( 'NONE', ( #68005, #94206, #5609, #86880 ) ) ;
#42835=CARTESIAN_POINT ( 'NONE',  ( -61.59189125704995860, -25.07259839747099051, 7.371166918563575976 ) ) ;
#42837=CARTESIAN_POINT ( 'NONE',  ( 14.30100545221680441, -14.83292283143518375, -1.500000000000002220 ) ) ;
#42838=ADVANCED_FACE ( 'NONE', ( #91789 ), #6060, .T. ) ;
#42839=CARTESIAN_POINT ( 'NONE',  ( -0.8629811567608781653, -21.54619324973139172, 11.49999999999999645 ) ) ;
#42844=CARTESIAN_POINT ( 'NONE',  ( -10.99827004860668822, -19.42154297629913628, 11.49999999999998934 ) ) ;
#42846=CARTESIAN_POINT ( 'NONE',  ( -0.07959803473139406838, -22.01954088903999107, 0.3010598746230624956 ) ) ;
#42847=DIRECTION ( 'NONE',  ( -1.000000000000000000, -3.773278334444166432E-23, -8.201307841325785021E-29 ) ) ;
#42849=ADVANCED_FACE ( 'NONE', ( #15167 ), #77557, .F. ) ;
#42851=CARTESIAN_POINT ( 'NONE',  ( -51.45240106148425241, -25.30046445047157633, 4.640179479081717240 ) ) ;
#42852=CARTESIAN_POINT ( 'NONE',  ( 20.34438994040483806, -4.565235006643893811, -1.500000000000002220 ) ) ;
#42853=EDGE_LOOP ( 'NONE', ( #43693, #39333, #74953, #35227 ) ) ;
#42858=DIRECTION ( 'NONE',  ( -0.000000000000000000, 2.173523156925979552E-06, -0.9999999999976378895 ) ) ;
#42859=CARTESIAN_POINT ( 'NONE',  ( -14.96386864383857329, 14.77685607883014640, -1.500000000000002220 ) ) ;
#42862=CARTESIAN_POINT ( 'NONE',  ( -48.97769291515528067, -25.29015023533645490, 5.627382122205519366 ) ) ;
#42863=CARTESIAN_POINT ( 'NONE',  ( -120.5910566015817551, -24.15602025860899360, 10.28564288303534902 ) ) ;
#42864=CARTESIAN_POINT ( 'NONE',  ( -80.96226385320382235, -25.13069340115295702, 2.947789388436138580 ) ) ;
#42865=DIRECTION ( 'NONE',  ( 0.000000000000000000, 2.173523156925980399E-06, -0.9999999999976378895 ) ) ;
#42866=CARTESIAN_POINT ( 'NONE',  ( -20.21959982808627032, -7.803091810188320210, -1.500000000000002220 ) ) ;
#42867=CARTESIAN_POINT ( 'NONE',  ( -80.52846833935618065, -25.12224391807531987, 7.100555464394792793 ) ) ;
#42868=CARTESIAN_POINT ( 'NONE',  ( 20.56042274393015035, -8.519965759701490171, 11.49999999999999645 ) ) ;
#42869=ORIENTED_EDGE ( 'NONE', *, *, #89580, .F. ) ;
#42870=CARTESIAN_POINT ( 'NONE',  ( -69.62287095715005592, -23.47596703998600631, 11.44779298504227683 ) ) ;
#42872=FACE_OUTER_BOUND ( 'NONE', #94012, .T. ) ;
#42873=ORIENTED_EDGE ( 'NONE', *, *, #93635, .F. ) ;
#42875=CARTESIAN_POINT ( 'NONE',  ( -40.62287095715004170, -24.63287334234176384, 0.9662140553045526215 ) ) ;
#42877=ORIENTED_EDGE ( 'NONE', *, *, #13912, .T. ) ;
#42878=CARTESIAN_POINT ( 'NONE',  ( -100.5775025149089572, -25.13380690292655828, 7.097842372401126809 ) ) ;
#42881=CARTESIAN_POINT ( 'NONE',  ( -80.62287095715004170, -23.48783264082478439, -1.443836473390065489 ) ) ;
#42882=EDGE_LOOP ( 'NONE', ( #67712, #80628, #86032, #43229 ) ) ;
#42883=CARTESIAN_POINT ( 'NONE',  ( -130.5728709571500872, -24.91553454762389208, 1.571120308003612687 ) ) ;
#42884=CARTESIAN_POINT ( 'NONE',  ( 9.841385673706204429, 20.17164819615926064, -1.500000000000002220 ) ) ;
#42886=CARTESIAN_POINT ( 'NONE',  ( -99.29687923781919778, -29.50249635395236325, 6.149702963151822743 ) ) ;
#42887=CARTESIAN_POINT ( 'NONE',  ( -94.60069879652984071, -23.48786465467241413, 11.44779295918254469 ) ) ;
#42890=CARTESIAN_POINT ( 'NONE',  ( -30.59799462776630108, -24.66513809378595568, 8.909134979017297340 ) ) ;
#42891=CARTESIAN_POINT ( 'NONE',  ( 5.347671334029483248, -18.86178030415664963, 11.49999999999998934 ) ) ;
#42892=CARTESIAN_POINT ( 'NONE',  ( -46.60715227236160274, -23.73766607897669800, -1.055555164236460008 ) ) ;
#42893=ORIENTED_EDGE ( 'NONE', *, *, #56660, .T. ) ;
#42894=AXIS2_PLACEMENT_3D ( 'NONE', #67863, #45524, #91179 ) ;
#42895=CARTESIAN_POINT ( 'NONE',  ( -11.62584540149672385, -18.10649092712023389, 11.49999999999998934 ) ) ;
#42896=B_SPLINE_CURVE_WITH_KNOTS ( 'NONE', 3,
 ( #15473, #22571, #31199, #6871 ),
 .UNSPECIFIED., .F., .F.,
 ( 4, 4 ),
 ( 0.000000000000000000, 9.999999999999592548E-05 ),
 .UNSPECIFIED. ) ;
#42898=CARTESIAN_POINT ( 'NONE',  ( -71.19450251067907232, -25.12219042401383007, 6.630762628979895545 ) ) ;
#42899=CARTESIAN_POINT ( 'NONE',  ( -100.5562042904833788, -23.48783264082478439, -1.443836473390062380 ) ) ;
#42901=CARTESIAN_POINT ( 'NONE',  ( 22.64363655503811046, -4.068770074275382953, -1.500000000000002220 ) ) ;
#42905=CARTESIAN_POINT ( 'NONE',  ( -53.57809818791832157, -24.65952944569304250, 1.056160979905695463 ) ) ;
#42906=CARTESIAN_POINT ( 'NONE',  ( 12.55954966114946458, -15.69740789531843461, 11.49999999999999645 ) ) ;
#42907=CARTESIAN_POINT ( 'NONE',  ( -56.52287095715009002, -23.48783264082476308, -1.443836473390091690 ) ) ;
#42908=CARTESIAN_POINT ( 'NONE',  ( -32.47727307158466914, -24.66019654487198665, 8.947790411086131712 ) ) ;
#42909=ADVANCED_FACE ( 'NONE', ( #92295 ), #30394, .T. ) ;
#42910=DIRECTION ( 'NONE',  ( -0.000000000000000000, 2.173523156925979552E-06, -0.9999999999976378895 ) ) ;
#42911=CARTESIAN_POINT ( 'NONE',  ( -113.5895376238167103, -23.48783264082479150, -1.443836473390060160 ) ) ;
#42912=CARTESIAN_POINT ( 'NONE',  ( -126.6228709571500559, -23.48786465467242124, 11.44779295918253403 ) ) ;
#42913=CARTESIAN_POINT ( 'NONE',  ( 6.283368587668265448, -18.83516890145298106, -1.500000000000002220 ) ) ;
#42914=CARTESIAN_POINT ( 'NONE',  ( -113.5222246106276884, -23.48783264082477373, -1.443836473390084807 ) ) ;
#42915=CARTESIAN_POINT ( 'NONE',  ( -16.18664964019209052, -11.25563402961023662, -1.500000000000002220 ) ) ;
#42916=EDGE_CURVE ( 'NONE', #16850, #63089, #37064, .T. ) ;
#42918=EDGE_CURVE ( 'NONE', #64205, #67134, #14054, .T. ) ;
#42919=B_SPLINE_CURVE_WITH_KNOTS ( 'NONE', 3,
 ( #14642, #76527, #7033, #86656, #9033, #38981, #39986, #22740 ),
 .UNSPECIFIED., .F., .F.,
 ( 4, 2, 2, 4 ),
 ( 0.000000000000000000, 0.002001079623178225828, 0.003001619434767337224, 0.004002159246356448187 ),
 .UNSPECIFIED. ) ;
#42921=EDGE_CURVE ( 'NONE', #33110, #27352, #91519, .T. ) ;
#42923=CARTESIAN_POINT ( 'NONE',  ( -79.52287095715004739, -24.33927499327855060, 9.819080762295811837 ) ) ;
#42924=CARTESIAN_POINT ( 'NONE',  ( 20.46650637700042097, -2.330123182410055893, 11.49999999999999645 ) ) ;
#42926=CARTESIAN_POINT ( 'NONE',  ( -42.62287095715004881, -23.48783264082477373, -1.443836473390072817 ) ) ;
#42927=CARTESIAN_POINT ( 'NONE',  ( -15.40814491850785650, 16.58152744545821022, 11.49999999999999645 ) ) ;
#42930=CARTESIAN_POINT ( 'NONE',  ( -102.5562042904833788, -24.65952944569305316, 1.056160979905701236 ) ) ;
#42931=CARTESIAN_POINT ( 'NONE',  ( -74.62287095715004170, -24.66019654487199375, 8.947790411086129936 ) ) ;
#42932=EDGE_CURVE ( 'NONE', #51201, #42129, #24777, .T. ) ;
#42933=CARTESIAN_POINT ( 'NONE',  ( -26.47413879005073056, -24.61460015870519058, 7.801149999016648628 ) ) ;
#42935=DIRECTION ( 'NONE',  ( 0.000000000000000000, -0.9999999999976377785, -2.173523156925979128E-06 ) ) ;
#42936=ORIENTED_EDGE ( 'NONE', *, *, #22208, .F. ) ;
#42937=ORIENTED_EDGE ( 'NONE', *, *, #37342, .T. ) ;
#42939=CARTESIAN_POINT ( 'NONE',  ( -99.36343569840310863, -25.21460787793245117, 6.488302719685625775 ) ) ;
#42940=CARTESIAN_POINT ( 'NONE',  ( 15.09361930729867574, -17.17024899132524496, -1.500000000000002220 ) ) ;
#42942=CARTESIAN_POINT ( 'NONE',  ( -17.67581969798968444, -12.36387604476075097, -1.500000000000002220 ) ) ;
#42945=CARTESIAN_POINT ( 'NONE',  ( -8.307687032909205627, 20.95097986170506488, 11.49999999999999645 ) ) ;
#42946=ORIENTED_EDGE ( 'NONE', *, *, #73179, .T. ) ;
#42947=CARTESIAN_POINT ( 'NONE',  ( -43.50598925632350245, -23.96119346886880308, -0.6495511937831988103 ) ) ;
#42948=CARTESIAN_POINT ( 'NONE',  ( -3.625624329714521643, -21.66436044012089468, 11.49999999999998934 ) ) ;
#42951=CARTESIAN_POINT ( 'NONE',  ( -118.5562042904834357, -23.48783264082479505, -1.443836473390058828 ) ) ;
#42953=CARTESIAN_POINT ( 'NONE',  ( -63.62287095715003460, -24.33927499327854704, 9.819080762295815390 ) ) ;
#42955=EDGE_LOOP ( 'NONE', ( #33818, #79424, #40915, #61322, #29120, #2746 ) ) ;
#42956=CARTESIAN_POINT ( 'NONE',  ( -77.62287095715005592, -23.72747288104441665, -1.053458166803662444 ) ) ;
#42957=EDGE_LOOP ( 'NONE', ( #89876, #98710, #26714, #90982 ) ) ;
#42958=VERTEX_POINT ( 'NONE', #48140 ) ;
#42960=CARTESIAN_POINT ( 'NONE',  ( -49.44228279013045579, -25.29936970972777033, 5.641479429678947888 ) ) ;
#42961=DIRECTION ( 'NONE',  ( -3.773278334453080206E-23, 0.9999999999976377785, 2.173523156925979975E-06 ) ) ;
#42963=CARTESIAN_POINT ( 'NONE',  ( 11.27307661227339430, 16.98952936956587934, -1.500000000000002220 ) ) ;
#42966=CARTESIAN_POINT ( 'NONE',  ( -29.48128483383218068, -24.42720452128061126, 9.386484716961749797 ) ) ;
#42967=EDGE_CURVE ( 'NONE', #32974, #28046, #29888, .T. ) ;
#42968=CARTESIAN_POINT ( 'NONE',  ( -105.6271250482996322, -24.63355581998386157, 0.9682620441943899925 ) ) ;
#42970=ORIENTED_EDGE ( 'NONE', *, *, #29050, .F. ) ;
#42972=CARTESIAN_POINT ( 'NONE',  ( -33.55620429048339304, -24.65952944569303895, 1.056160979905688801 ) ) ;
#42975=CARTESIAN_POINT ( 'NONE',  ( -20.76960556195881225, -0.3855258213679747525, -1.500000000000002220 ) ) ;
#42977=ORIENTED_EDGE ( 'NONE', *, *, #36548, .F. ) ;
#42981=CARTESIAN_POINT ( 'NONE',  ( -51.90571684870070612, -25.27193873804239033, 5.908765195229332079 ) ) ;
#42983=ORIENTED_EDGE ( 'NONE', *, *, #6344, .T. ) ;
#42987=B_SPLINE_CURVE_WITH_KNOTS ( 'NONE', 3,
 ( #70366, #62264, #93189, #70876 ),
 .UNSPECIFIED., .F., .F.,
 ( 4, 4 ),
 ( 7.248525107586175442E-06, 0.001219383299454008997 ),
 .UNSPECIFIED. ) ;
#42988=CARTESIAN_POINT ( 'NONE',  ( -43.59362069740146950, -24.15620529776627379, 10.23563542870661180 ) ) ;
#42989=CARTESIAN_POINT ( 'NONE',  ( 0.6065052782250800467, 22.08157775750015617, 11.49999999999999645 ) ) ;
#42992=CARTESIAN_POINT ( 'NONE',  ( -2.075279548881721947, -22.52154899835045043, 11.49999999999998934 ) ) ;
#42993=CARTESIAN_POINT ( 'NONE',  ( -115.5155043013981953, -24.63419186844613051, 9.035850630976920428 ) ) ;
#42994=EDGE_LOOP ( 'NONE', ( #89243, #75395, #15297, #59118 ) ) ;
#42995=ORIENTED_EDGE ( 'NONE', *, *, #77247, .F. ) ;
#42996=CARTESIAN_POINT ( 'NONE',  ( -80.60277405640064785, -25.31556075360760261, 4.974435291001888082 ) ) ;
#42998=CARTESIAN_POINT ( 'NONE',  ( -42.52287095715005449, -24.64898659630367206, 1.056161002820819261 ) ) ;
#43000=CARTESIAN_POINT ( 'NONE',  ( -6.202713861520617655, -20.23501359363181962, 11.49999999999998934 ) ) ;
#43002=DIRECTION ( 'NONE',  ( -3.773278334453079030E-23, 0.9999999999976377785, 2.173523156925979128E-06 ) ) ;
#43003=CARTESIAN_POINT ( 'NONE',  ( 17.40631026334068565, 13.93540124644318645, -1.500000000000002220 ) ) ;
#43004=PLANE ( 'NONE',  #85693 ) ;
#43005=AXIS2_PLACEMENT_3D ( 'NONE', #85010, #15494, #22107 ) ;
#43007=CARTESIAN_POINT ( 'NONE',  ( -78.55620429048339304, -23.47593901973091235, -1.443836447539004642 ) ) ;
#43008=CARTESIAN_POINT ( 'NONE',  ( -48.55620429048338593, -24.65952944569304606, 1.056160979905694797 ) ) ;
#43009=AXIS2_PLACEMENT_3D ( 'NONE', #32830, #54675, #17603 ) ;
#43010=CARTESIAN_POINT ( 'NONE',  ( -29.52287095715006160, -23.38909342368989641, 11.44779306042727285 ) ) ;
#43011=B_SPLINE_CURVE_WITH_KNOTS ( 'NONE', 3,
 ( #69846, #9940, #1340, #40398, #1840, #71854 ),
 .UNSPECIFIED., .F., .F.,
 ( 4, 2, 4 ),
 ( 6.384118694913733240E-06, 0.001386860460836522764, 0.002767336802978131484 ),
 .UNSPECIFIED. ) ;
#43012=CARTESIAN_POINT ( 'NONE',  ( -45.22287095715005023, -23.47596703998600276, 11.44779298504227683 ) ) ;
#43013=CARTESIAN_POINT ( 'NONE',  ( 10.93668938013857783, -16.14717738681254033, 11.49999999999998934 ) ) ;
#43014=CARTESIAN_POINT ( 'NONE',  ( 21.23773461148298836, -3.020459416520930862, 11.49999999999998934 ) ) ;
#43016=CARTESIAN_POINT ( 'NONE',  ( -108.6228709571500417, -23.48786465467242479, 11.44779295918253759 ) ) ;
#43017=CARTESIAN_POINT ( 'NONE',  ( -77.59210467935486122, -24.15543982623907482, -0.2315651400026658147 ) ) ;
#43018=CARTESIAN_POINT ( 'NONE',  ( -19.65108876255925807, -11.61119296138784662, -1.500000000000002220 ) ) ;
#43019=CARTESIAN_POINT ( 'NONE',  ( -39.52287095715007581, -23.72747288104470087, -1.053458166803227680 ) ) ;
#43020=DIRECTION ( 'NONE',  ( 3.773278334444167608E-23, -1.000000000000000000, 0.000000000000000000 ) ) ;
#43021=CARTESIAN_POINT ( 'NONE',  ( 7.614665684681447111, -18.39110272641453037, 11.49999999999999645 ) ) ;
#43022=CARTESIAN_POINT ( 'NONE',  ( -104.5196659495136657, -23.73766607897670866, -1.055555164236449572 ) ) ;
#43024=ADVANCED_FACE ( 'NONE', ( #1462 ), #16669, .T. ) ;
#43026=CARTESIAN_POINT ( 'NONE',  ( -76.58953762381673869, -23.47596703998600276, 11.44779298504227683 ) ) ;
#43027=EDGE_LOOP ( 'NONE', ( #28310, #54967, #56570, #82748 ) ) ;
#43028=DIRECTION ( 'NONE',  ( 3.773278334444167608E-23, -1.000000000000000000, 0.000000000000000000 ) ) ;
#43029=CARTESIAN_POINT ( 'NONE',  ( -31.22214303690239134, -25.16202561908117730, 2.791798636425737445 ) ) ;
#43031=CARTESIAN_POINT ( 'NONE',  ( -6.179238894844691465, -20.81818906610659425, 11.49999999999998934 ) ) ;
#43033=CARTESIAN_POINT ( 'NONE',  ( 10.86043079284791091, -16.25897383129715834, -1.500000000000002220 ) ) ;
#43034=ADVANCED_FACE ( 'NONE', ( #40527 ), #47138, .T. ) ;
#43035=CARTESIAN_POINT ( 'NONE',  ( -55.66784890944978059, -23.48786465467241058, 11.44779295918254647 ) ) ;
#43038=AXIS2_PLACEMENT_3D ( 'NONE', #85209, #38536, #61892 ) ;
#43039=CARTESIAN_POINT ( 'NONE',  ( -112.5228709571500616, -29.50250243563736774, 8.947779886222136270 ) ) ;
#43040=CARTESIAN_POINT ( 'NONE',  ( 9.418145840992488971, -18.15903486995133065, 11.49999999999999645 ) ) ;
#43042=CARTESIAN_POINT ( 'NONE',  ( -86.52287095715006160, -24.64965694238575011, 8.947790433994196491 ) ) ;
#43043=EDGE_CURVE ( 'NONE', #61226, #96695, #52895, .T. ) ;
#43044=ORIENTED_EDGE ( 'NONE', *, *, #63206, .F. ) ;
#43047=DIRECTION ( 'NONE',  ( -1.000000000000000000, -3.773278334444166432E-23, -8.201307841325785021E-29 ) ) ;
#43048=B_SPLINE_CURVE_WITH_KNOTS ( 'NONE', 3,
 ( #59356, #20771, #36011, #90301, #60865, #7062 ),
 .UNSPECIFIED., .F., .F.,
 ( 4, 2, 4 ),
 ( 6.391158118964604309E-06, 0.001387004593080786580, 0.002767618028042608501 ),
 .UNSPECIFIED. ) ;
#43049=CARTESIAN_POINT ( 'NONE',  ( -108.5228709571500616, -23.48786465467241769, 11.44779295918253936 ) ) ;
#43052=CARTESIAN_POINT ( 'NONE',  ( 22.97298546869389568, 1.202750762487129199, 11.49999999999999645 ) ) ;
#43053=CARTESIAN_POINT ( 'NONE',  ( 0.9741843557120299923, -22.74547949729550922, -1.500000000000002220 ) ) ;
#43055=CARTESIAN_POINT ( 'NONE',  ( -93.92287095715012413, -23.47593901973090880, -1.443836447538997314 ) ) ;
#43058=CARTESIAN_POINT ( 'NONE',  ( -63.52287095715006160, -29.50248528299804818, 1.056150453629034924 ) ) ;
#43059=CARTESIAN_POINT ( 'NONE',  ( -21.47987282208850601, -4.139150239982721580, -1.500000000000002220 ) ) ;
#43062=CARTESIAN_POINT ( 'NONE',  ( -34.62287095715005592, -24.64965695001467694, 8.947790433994189385 ) ) ;
#43064=CARTESIAN_POINT ( 'NONE',  ( -58.63232380827055579, -24.34968618360933945, 0.1864209137778795045 ) ) ;
#43066=CARTESIAN_POINT ( 'NONE',  ( -15.93830457579706739, -12.76012858937699335, -1.500000000000002220 ) ) ;
#43067=ORIENTED_EDGE ( 'NONE', *, *, #31016, .T. ) ;
#43068=VECTOR ( 'NONE', #54860, 1000.000000000000114 ) ;
#43070=EDGE_LOOP ( 'NONE', ( #11533, #69880, #60314, #28457 ) ) ;
#43071=ORIENTED_EDGE ( 'NONE', *, *, #89960, .F. ) ;
#43072=CARTESIAN_POINT ( 'NONE',  ( -1.973530150111237003, 22.95712487800313539, 11.49999999999998934 ) ) ;
#43074=CARTESIAN_POINT ( 'NONE',  ( 14.71488472389458124, -13.84269218943631508, -1.500000000000002220 ) ) ;
#43076=ORIENTED_EDGE ( 'NONE', *, *, #48085, .F. ) ;
#43077=EDGE_CURVE ( 'NONE', #65310, #35855, #52707, .T. ) ;
#43078=LINE ( 'NONE', #96356, #94704 ) ;
#43081=CARTESIAN_POINT ( 'NONE',  ( -95.63175277689521181, -24.40034930558991633, 0.3402023900116099009 ) ) ;
#43082=PLANE ( 'NONE',  #31834 ) ;
#43083=CARTESIAN_POINT ( 'NONE',  ( 6.831138157384286203, 20.27010762675863731, 11.49999999999999645 ) ) ;
#43084=ORIENTED_EDGE ( 'NONE', *, *, #28242, .T. ) ;
#43086=ORIENTED_EDGE ( 'NONE', *, *, #99459, .T. ) ;
#43087=CARTESIAN_POINT ( 'NONE',  ( 5.670930919660429836, -21.52877996283707418, 11.49999999999998934 ) ) ;
#43088=B_SPLINE_CURVE_WITH_KNOTS ( 'NONE', 3,
 ( #86471, #57048, #63152, #1250 ),
 .UNSPECIFIED., .F., .F.,
 ( 4, 4 ),
 ( 0.000000000000000000, 9.999999999998897304E-05 ),
 .UNSPECIFIED. ) ;
#43089=CARTESIAN_POINT ( 'NONE',  ( -20.55277978778089576, -2.218614319624547360, -1.500000000000002220 ) ) ;
#43091=ORIENTED_EDGE ( 'NONE', *, *, #53893, .T. ) ;
#43093=ORIENTED_EDGE ( 'NONE', *, *, #67681, .F. ) ;
#43094=CARTESIAN_POINT ( 'NONE',  ( -129.5228709571499905, -24.50216790748206819, 0.6166512839542598323 ) ) ;
#43095=ORIENTED_EDGE ( 'NONE', *, *, #70924, .T. ) ;
#43097=CARTESIAN_POINT ( 'NONE',  ( -15.06743543786183714, 14.52697759824333090, -1.500000000000002220 ) ) ;
#43098=CARTESIAN_POINT ( 'NONE',  ( -21.55542221127511482, -4.010009934288176758, 11.49999999999999645 ) ) ;
#43099=CARTESIAN_POINT ( 'NONE',  ( -37.52762035705108445, -24.66019654487199730, 8.947790411086113949 ) ) ;
#43100=CARTESIAN_POINT ( 'NONE',  ( -1.797493081057526032, -22.44471576765463183, 11.49999999999998934 ) ) ;
#43101=CARTESIAN_POINT ( 'NONE',  ( 5.581485548573628996, 20.18083795961418403, -1.500000000000002220 ) ) ;
#43102=CARTESIAN_POINT ( 'NONE',  ( -26.09708441595108397, -24.88148730279706911, 5.016021623328582812 ) ) ;
#43103=CARTESIAN_POINT ( 'NONE',  ( -57.62287095715004881, -29.50247984919015209, -1.443849546365056913 ) ) ;
#43104=CARTESIAN_POINT ( 'NONE',  ( -119.6241211350181715, -24.51419770103158768, 9.386484678747159194 ) ) ;
#43108=ORIENTED_EDGE ( 'NONE', *, *, #62915, .T. ) ;
#43109=CARTESIAN_POINT ( 'NONE',  ( -66.63133949696768354, -24.34968618360933235, 0.1864209137778773395 ) ) ;
#43110=ORIENTED_EDGE ( 'NONE', *, *, #60776, .T. ) ;
#43111=CARTESIAN_POINT ( 'NONE',  ( -7.042111407433782055, -20.27750348750624099, -1.500000000000002220 ) ) ;
#43113=EDGE_LOOP ( 'NONE', ( #83999, #19252, #62424, #69665 ) ) ;
#43114=CARTESIAN_POINT ( 'NONE',  ( -12.45680796028966597, 17.00782699154285638, -1.500000000000002220 ) ) ;
#43115=CARTESIAN_POINT ( 'NONE',  ( -115.6228709571500701, -25.00158670708909625, 2.256160236439165967 ) ) ;
#43117=CARTESIAN_POINT ( 'NONE',  ( -50.62120248232606912, -23.48786465467240347, 11.44779295918255002 ) ) ;
#43119=CARTESIAN_POINT ( 'NONE',  ( -100.5895376238167245, -24.99132157543167310, 2.256160258750668390 ) ) ;
#43120=CARTESIAN_POINT ( 'NONE',  ( 19.10104996495751450, -11.12853483292915691, -1.500000000000002220 ) ) ;
#43122=FACE_OUTER_BOUND ( 'NONE', #65656, .T. ) ;
#43124=CARTESIAN_POINT ( 'NONE',  ( -40.49165087243459737, -25.31624741777496013, 5.543942831290165074 ) ) ;
#43125=VECTOR ( 'NONE', #80966, 1000.000000000000114 ) ;
#43126=EDGE_CURVE ( 'NONE', #46989, #30992, #97788, .T. ) ;
#43127=CARTESIAN_POINT ( 'NONE',  ( -62.62365721985609213, -24.66019654487199730, 8.947790411086124607 ) ) ;
#43129=CARTESIAN_POINT ( 'NONE',  ( 5.124585555570928541, 20.71496159572455653, 11.49999999999998934 ) ) ;
#43130=CARTESIAN_POINT ( 'NONE',  ( -68.94617923632279144, -25.23882047181962918, 6.370111357818270648 ) ) ;
#43131=CARTESIAN_POINT ( 'NONE',  ( -48.85424939675955613, -25.30060005375480969, 6.009289253917325269 ) ) ;
#43133=CARTESIAN_POINT ( 'NONE',  ( -67.62287095715004170, -24.66019654487199020, 8.947790411086131712 ) ) ;
#43134=CARTESIAN_POINT ( 'NONE',  ( -6.441999407266626676, 21.70310835763521595, -1.500000000000002220 ) ) ;
#43136=B_SPLINE_CURVE_WITH_KNOTS ( 'NONE', 3,
 ( #76991, #69897, #1399, #46563, #61799, #47574 ),
 .UNSPECIFIED., .F., .F.,
 ( 4, 2, 4 ),
 ( 0.000000000000000000, 0.001380764517854764966, 0.002761529035709529931 ),
 .UNSPECIFIED. ) ;
#43137=DIRECTION ( 'NONE',  ( -3.773278334453080206E-23, 0.9999999999976377785, 2.173523156925979975E-06 ) ) ;
#43139=AXIS2_PLACEMENT_3D ( 'NONE', #15746, #77634, #8145 ) ;
#43142=CARTESIAN_POINT ( 'NONE',  ( -18.24397684793207830, 7.494555614300850266, 11.49999999999999645 ) ) ;
#43143=FACE_OUTER_BOUND ( 'NONE', #27245, .T. ) ;
#43144=EDGE_CURVE ( 'NONE', #71294, #34495, #73466, .T. ) ;
#43145=AXIS2_PLACEMENT_3D ( 'NONE', #81824, #3714, #66628 ) ;
#43146=CARTESIAN_POINT ( 'NONE',  ( -73.52287095715006160, -24.50321055353805733, 9.387540953477529371 ) ) ;
#43149=CARTESIAN_POINT ( 'NONE',  ( -45.52287095715006160, -29.50250243563736774, 8.947779886222146928 ) ) ;
#43150=CARTESIAN_POINT ( 'NONE',  ( -70.52287095715007581, -24.52323809116983711, 9.355190652339418378 ) ) ;
#43151=ADVANCED_FACE ( 'NONE', ( #59239 ), #28280, .T. ) ;
#43152=CARTESIAN_POINT ( 'NONE',  ( -75.52287095715007581, -24.63345952396255356, 9.038047939301504741 ) ) ;
#43153=CARTESIAN_POINT ( 'NONE',  ( 7.158504886898216846, -20.39052948596947346, 11.49999999999998934 ) ) ;
#43154=FACE_OUTER_BOUND ( 'NONE', #14092, .T. ) ;
#43156=CARTESIAN_POINT ( 'NONE',  ( 7.305494252837257285, 17.95555029072639286, -1.500000000000002220 ) ) ;
#43159=PLANE ( 'NONE',  #13398 ) ;
#43160=CARTESIAN_POINT ( 'NONE',  ( 2.545096341412688812, 19.61957628810408849, -1.500000000000002220 ) ) ;
#43161=ORIENTED_EDGE ( 'NONE', *, *, #63767, .F. ) ;
#43163=CARTESIAN_POINT ( 'NONE',  ( 14.61151973098085222, 14.07909450314327771, 11.49999999999999645 ) ) ;
#43167=ORIENTED_EDGE ( 'NONE', *, *, #79311, .F. ) ;
#43170=DIRECTION ( 'NONE',  ( -3.773278334444166432E-23, 1.000000000000000000, 0.000000000000000000 ) ) ;
#43172=CARTESIAN_POINT ( 'NONE',  ( -31.52287095715006160, -23.47596703998600631, 11.44779298504229459 ) ) ;
#43173=CARTESIAN_POINT ( 'NONE',  ( 8.743921044546416610, -18.04861246754477477, 11.49999999999998934 ) ) ;
#43176=EDGE_LOOP ( 'NONE', ( #4156, #23973, #73406, #96383 ) ) ;
#43179=CARTESIAN_POINT ( 'NONE',  ( -115.5562042904833646, -23.48783264082478794, -1.443836473390058384 ) ) ;
#43180=DIRECTION ( 'NONE',  ( 1.000000000000000000, 3.773278334444166432E-23, 8.201307841325785021E-29 ) ) ;
#43181=B_SPLINE_CURVE_WITH_KNOTS ( 'NONE', 3,
 ( #10562, #19663, #2970, #96800 ),
 .UNSPECIFIED., .F., .F.,
 ( 4, 4 ),
 ( 1.387778780781445521E-17, 9.999999999997510880E-05 ),
 .UNSPECIFIED. ) ;
#43182=LINE ( 'NONE', #57417, #30220 ) ;
#43183=B_SPLINE_CURVE_WITH_KNOTS ( 'NONE', 3,
 ( #27236, #58191, #67298, #21099, #68288, #74884 ),
 .UNSPECIFIED., .F., .F.,
 ( 4, 2, 4 ),
 ( 6.391158118967745954E-06, 0.001387004593080788098, 0.002767618028042608501 ),
 .UNSPECIFIED. ) ;
#43184=CARTESIAN_POINT ( 'NONE',  ( -120.6228709571500417, -23.48783264082479505, -1.443836473390058384 ) ) ;
#43185=CARTESIAN_POINT ( 'NONE',  ( -93.55620429048336462, -24.64898659630528854, 1.056161002820828143 ) ) ;
#43186=VERTEX_POINT ( 'NONE', #74456 ) ;
#43187=CARTESIAN_POINT ( 'NONE',  ( 16.70477854660759931, 11.60849435585976153, -1.500000000000002220 ) ) ;
#43188=ORIENTED_EDGE ( 'NONE', *, *, #59167, .F. ) ;
#43190=CARTESIAN_POINT ( 'NONE',  ( -22.24355531667433539, 5.575215412481045796, -1.500000000000002220 ) ) ;
#43193=CARTESIAN_POINT ( 'NONE',  ( -111.6228709571500559, -24.64898659630368627, 1.056161002820831474 ) ) ;
#43195=CARTESIAN_POINT ( 'NONE',  ( -76.52287095715006160, -23.72747288104470087, -1.053458166803226348 ) ) ;
#43197=CARTESIAN_POINT ( 'NONE',  ( -87.58953762381671027, -24.64898659630528854, 1.056161002820826811 ) ) ;
#43198=CARTESIAN_POINT ( 'NONE',  ( -1.563627757057377110, -21.15500258984412696, 11.49999999999999645 ) ) ;
#43199=CARTESIAN_POINT ( 'NONE',  ( -14.73459587841175633, -16.56598928932902837, -1.500000000000002220 ) ) ;
#43200=CARTESIAN_POINT ( 'NONE',  ( 15.34425395324244867, 13.73259486114767114, 11.49999999999998934 ) ) ;
#43201=AXIS2_PLACEMENT_3D ( 'NONE', #99541, #52901, #77206 ) ;
#43202=ORIENTED_EDGE ( 'NONE', *, *, #7100, .T. ) ;
#43203=VERTEX_POINT ( 'NONE', #64886 ) ;
#43204=LINE ( 'NONE', #66564, #44668 ) ;
#43206=CARTESIAN_POINT ( 'NONE',  ( -50.52287095715006160, -24.91570333825769978, 8.075032458260348989 ) ) ;
#43207=ORIENTED_EDGE ( 'NONE', *, *, #92352, .T. ) ;
#43209=ORIENTED_EDGE ( 'NONE', *, *, #78635, .F. ) ;
#43211=EDGE_LOOP ( 'NONE', ( #16119, #11242, #77360, #1892 ) ) ;
#43213=CARTESIAN_POINT ( 'NONE',  ( -28.53657574427005272, -24.19026137835766121, 9.817618374534074377 ) ) ;
#43215=CARTESIAN_POINT ( 'NONE',  ( 3.485566553294195291, 20.44204155273375889, -1.500000000000002220 ) ) ;
#43216=CARTESIAN_POINT ( 'NONE',  ( 12.24854465327799424, 17.96525243877979605, 11.49999999999999645 ) ) ;
#43217=EDGE_CURVE ( 'NONE', #25435, #32470, #82069, .T. ) ;
#43219=LINE ( 'NONE', #51827, #23979 ) ;
#43220=CARTESIAN_POINT ( 'NONE',  ( -119.6228709571500559, -23.73934037231757799, 11.05740245334327554 ) ) ;
#43221=CARTESIAN_POINT ( 'NONE',  ( 21.09243369641204069, 7.689775423913054908, -1.500000000000002220 ) ) ;
#43226=FACE_OUTER_BOUND ( 'NONE', #39136, .T. ) ;
#43227=DIRECTION ( 'NONE',  ( 0.000000000000000000, -2.173523156925979552E-06, 0.9999999999976378895 ) ) ;
#43228=ORIENTED_EDGE ( 'NONE', *, *, #82647, .T. ) ;
#43229=ORIENTED_EDGE ( 'NONE', *, *, #85675, .T. ) ;
#43233=CARTESIAN_POINT ( 'NONE',  ( -20.86817740539179056, 4.147639786170328691, -1.500000000000002220 ) ) ;
#43234=ORIENTED_EDGE ( 'NONE', *, *, #13810, .T. ) ;
#43235=CARTESIAN_POINT ( 'NONE',  ( -103.6228709571500559, -23.48786465467241769, 11.44779295918254114 ) ) ;
#43236=CARTESIAN_POINT ( 'NONE',  ( 19.95399986947220583, -8.914707708046476498, -1.500000000000002220 ) ) ;
#43238=CARTESIAN_POINT ( 'NONE',  ( 22.47986593085892437, -3.190245585651162230, -1.500000000000002220 ) ) ;
#43239=B_SPLINE_CURVE_WITH_KNOTS ( 'NONE', 3,
 ( #20929, #61514, #36173, #75708 ),
 .UNSPECIFIED., .F., .F.,
 ( 4, 4 ),
 ( 0.7603288567031503131, 0.7693352879752661799 ),
 .UNSPECIFIED. ) ;
#43240=DIRECTION ( 'NONE',  ( 0.000000000000000000, 0.9999999999976377785, 2.173523156925979128E-06 ) ) ;
#43241=DIRECTION ( 'NONE',  ( 3.773278334444167608E-23, -1.000000000000000000, 0.000000000000000000 ) ) ;
#43242=CARTESIAN_POINT ( 'NONE',  ( 14.12621959167996977, 16.79361087625908056, -1.500000000000002220 ) ) ;
#43245=CARTESIAN_POINT ( 'NONE',  ( -122.5551195424030340, -24.15620529776629510, 10.23563542870659582 ) ) ;
#43246=CARTESIAN_POINT ( 'NONE',  ( -127.6228709571500559, -29.50247984919015209, -1.443849546365044922 ) ) ;
#43248=ORIENTED_EDGE ( 'NONE', *, *, #41131, .T. ) ;
#43249=CARTESIAN_POINT ( 'NONE',  ( -30.64751926837171325, -23.47596703998600631, 11.44779298504228038 ) ) ;
#43252=CARTESIAN_POINT ( 'NONE',  ( -30.58080508546457210, -25.30587485921815016, 3.856996771330998719 ) ) ;
#43253=CARTESIAN_POINT ( 'NONE',  ( 14.70648301983428397, -15.34743991077593250, 11.49999999999998934 ) ) ;
#43254=CARTESIAN_POINT ( 'NONE',  ( -112.6299549673751272, -23.73766607897671577, -1.055555164236427590 ) ) ;
#43255=CARTESIAN_POINT ( 'NONE',  ( -26.92257395956520938, -24.97064456621790640, 2.526139883312569889 ) ) ;
#43256=PLANE ( 'NONE',  #71299 ) ;
#43257=CARTESIAN_POINT ( 'NONE',  ( -84.62287095715009855, -24.35013146730204525, 9.818937971375111928 ) ) ;
#43258=CARTESIAN_POINT ( 'NONE',  ( -35.52287095715006870, -29.50250786944525672, 11.44777988621624232 ) ) ;
#43259=ORIENTED_EDGE ( 'NONE', *, *, #60356, .T. ) ;
#43260=CARTESIAN_POINT ( 'NONE',  ( 6.425176733589397671, 18.50107501292125178, 11.49999999999999645 ) ) ;
#43261=CARTESIAN_POINT ( 'NONE',  ( -130.5728709571500588, -23.47593901973090524, -1.443836447538995982 ) ) ;
#43262=EDGE_CURVE ( 'NONE', #85507, #81379, #79288, .T. ) ;
#43266=CARTESIAN_POINT ( 'NONE',  ( -99.29884676835234814, -25.25095974635953056, 6.107783339703508396 ) ) ;
#43267=AXIS2_PLACEMENT_3D ( 'NONE', #92888, #46733, #47232 ) ;
#43268=CARTESIAN_POINT ( 'NONE',  ( -62.52287095715006160, -23.48786465467241058, 11.44779295918254824 ) ) ;
#43270=CARTESIAN_POINT ( 'NONE',  ( 11.88433821776028942, -15.71472908967258242, 11.49999999999998934 ) ) ;
#43274=FACE_OUTER_BOUND ( 'NONE', #83964, .T. ) ;
#43275=EDGE_CURVE ( 'NONE', #28558, #55465, #27374, .T. ) ;
#43276=VECTOR ( 'NONE', #87612, 1000.000000000000114 ) ;
#43278=ORIENTED_EDGE ( 'NONE', *, *, #31347, .F. ) ;
#43280=CARTESIAN_POINT ( 'NONE',  ( -105.6228709571500417, -24.99156045073393173, 7.747789690856161648 ) ) ;
#43281=CARTESIAN_POINT ( 'NONE',  ( -69.62287095715005592, -23.47593901973091235, -1.443836447539006196 ) ) ;
#43283=CARTESIAN_POINT ( 'NONE',  ( -49.62287095715005592, -24.64965695001467694, 8.947790433994185832 ) ) ;
#43287=DIRECTION ( 'NONE',  ( -3.773278334453079618E-23, 0.9999999999976377785, 2.173523156925979975E-06 ) ) ;
#43288=CARTESIAN_POINT ( 'NONE',  ( 16.68016870136555596, 10.92824754362290385, 11.49999999999998934 ) ) ;
#43291=CARTESIAN_POINT ( 'NONE',  ( -0.07754179015905204864, -22.04616059090901103, 0.1112944789973146359 ) ) ;
#43296=CARTESIAN_POINT ( 'NONE',  ( -45.62287095715004881, -23.47596703998600276, 11.44779298504227505 ) ) ;
#43297=CARTESIAN_POINT ( 'NONE',  ( -35.92287095715005307, -23.47593901973090169, -1.443836447538997980 ) ) ;
#43298=CARTESIAN_POINT ( 'NONE',  ( -100.6814946224345562, -25.31603993156367949, 4.890060501307835317 ) ) ;
#43299=CARTESIAN_POINT ( 'NONE',  ( -51.29010191576745115, -25.25452040107872520, 3.888211261899670035 ) ) ;
#43300=ORIENTED_EDGE ( 'NONE', *, *, #62784, .T. ) ;
#43301=CARTESIAN_POINT ( 'NONE',  ( -62.62287095715004881, -23.47593901973091235, -1.443836447539007972 ) ) ;
#43302=CARTESIAN_POINT ( 'NONE',  ( -52.52287095715006870, -29.50250243563736774, 8.947779886222146928 ) ) ;
#43304=CARTESIAN_POINT ( 'NONE',  ( 20.17645099164838030, 1.678240329834772115, -1.500000000000002220 ) ) ;
#43305=CARTESIAN_POINT ( 'NONE',  ( -70.09747585296138084, -25.31475305677228249, 4.859175633302561970 ) ) ;
#43307=VECTOR ( 'NONE', #4173, 1000.000000000000227 ) ;
#43310=CARTESIAN_POINT ( 'NONE',  ( -46.62287095715006302, -24.33927499327855060, 9.819080762295818943 ) ) ;
#43312=FACE_OUTER_BOUND ( 'NONE', #23824, .T. ) ;
#43313=CARTESIAN_POINT ( 'NONE',  ( -18.39468835979788608, -8.022455445098881199, -1.500000000000002220 ) ) ;
#43314=CARTESIAN_POINT ( 'NONE',  ( 20.92198360912786015, -1.804805560479522342, 11.49999999999999645 ) ) ;
#43317=CARTESIAN_POINT ( 'NONE',  ( -70.64337588465900808, -24.15602025860896518, 10.28564288303534724 ) ) ;
#43318=CARTESIAN_POINT ( 'NONE',  ( -19.65368394218270254, -10.04821906498216499, 11.49999999999998934 ) ) ;
#43320=CARTESIAN_POINT ( 'NONE',  ( -127.6228709571500559, -23.47596703998600631, 11.44779298504227860 ) ) ;
#43322=CARTESIAN_POINT ( 'NONE',  ( -96.52287095715006160, -24.65952944569304606, 1.056160979905702346 ) ) ;
#43324=EDGE_LOOP ( 'NONE', ( #70599, #54450, #19216, #60420 ) ) ;
#43325=CARTESIAN_POINT ( 'NONE',  ( -35.52287095715007581, -24.92604778743017135, 8.074972756849357225 ) ) ;
#43326=CARTESIAN_POINT ( 'NONE',  ( -31.53772339877937370, -24.34968618360933590, 0.1864209137778850556 ) ) ;
#43328=ORIENTED_EDGE ( 'NONE', *, *, #29252, .T. ) ;
#43331=CARTESIAN_POINT ( 'NONE',  ( -89.62287095715007013, -24.34917612406837861, 0.1852690917426663697 ) ) ;
#43332=CARTESIAN_POINT ( 'NONE',  ( 1.582324178664715975, -20.54890914157308401, -1.500000000000002220 ) ) ;
#43333=CARTESIAN_POINT ( 'NONE',  ( -5.754811884962036217, -20.78327508566754389, 11.49999999999999645 ) ) ;
#43334=EDGE_LOOP ( 'NONE', ( #10364, #73522, #41112, #40489 ) ) ;
#43336=CARTESIAN_POINT ( 'NONE',  ( -71.62287095715005592, -29.50247984919015209, -1.443849546365055359 ) ) ;
#43337=CARTESIAN_POINT ( 'NONE',  ( -97.62287095715005592, -23.48783264082478794, -1.443836473390061936 ) ) ;
#43338=CARTESIAN_POINT ( 'NONE',  ( -14.53400517605410158, 16.95891092046126403, 11.49999999999998934 ) ) ;
#43339=AXIS2_PLACEMENT_3D ( 'NONE', #30250, #53114, #45502 ) ;
#43341=CARTESIAN_POINT ( 'NONE',  ( -127.6228709571500559, -24.64898659630368627, 1.056161002820834804 ) ) ;
#43343=CARTESIAN_POINT ( 'NONE',  ( -94.52287095715003318, -24.51283580621365488, 0.6167428607019757036 ) ) ;
#43344=CARTESIAN_POINT ( 'NONE',  ( -89.40841769935767047, -29.50249691823240994, 6.409318347766594037 ) ) ;
#43345=CARTESIAN_POINT ( 'NONE',  ( -19.94048968823238255, 6.179419890754223488, -1.500000000000002220 ) ) ;
#43351=EDGE_CURVE ( 'NONE', #27247, #95575, #90266, .T. ) ;
#43352=ORIENTED_EDGE ( 'NONE', *, *, #49113, .F. ) ;
#43353=FACE_OUTER_BOUND ( 'NONE', #15397, .T. ) ;
#43354=CARTESIAN_POINT ( 'NONE',  ( 14.88031740681034698, -14.96734982212533183, -1.500000000000002220 ) ) ;
#43355=VERTEX_POINT ( 'NONE', #75940 ) ;
#43356=CARTESIAN_POINT ( 'NONE',  ( -28.52287095715006515, -23.56402623438133404, -1.053577192903873527 ) ) ;
#43357=CARTESIAN_POINT ( 'NONE',  ( -124.6228709571500559, -23.48786465467241769, 11.44779295918253759 ) ) ;
#43358=CARTESIAN_POINT ( 'NONE',  ( -61.62287095715004881, -23.48786465467240347, 11.44779295918254824 ) ) ;
#43360=CARTESIAN_POINT ( 'NONE',  ( -76.49746590141513991, -24.66019654487199375, 8.947790411086119278 ) ) ;
#43361=DIRECTION ( 'NONE',  ( 0.000000000000000000, 0.9999999999976377785, 2.173523156925979975E-06 ) ) ;
#43362=CARTESIAN_POINT ( 'NONE',  ( 0.2638585030419089428, -21.76204025362994798, -1.500000000000002220 ) ) ;
#43363=CARTESIAN_POINT ( 'NONE',  ( -81.29833273411215089, -25.24759724262089833, 6.730504689138452790 ) ) ;
#43364=CARTESIAN_POINT ( 'NONE',  ( 22.08996893241407378, 3.065900275835479860, 11.49999999999999645 ) ) ;
#43366=CARTESIAN_POINT ( 'NONE',  ( -33.52287095715007581, -23.48783264083359512, -1.443836473376374441 ) ) ;
#43368=CARTESIAN_POINT ( 'NONE',  ( -57.62287095715004881, -29.50247984919015209, -1.443849546365056913 ) ) ;
#43370=ADVANCED_FACE ( 'NONE', ( #60745 ), #98778, .T. ) ;
#43371=EDGE_CURVE ( 'NONE', #69024, #37139, #87749, .T. ) ;
#43372=CARTESIAN_POINT ( 'NONE',  ( -54.52287095715005449, -23.47593901973090169, -1.443836447538997092 ) ) ;
#43373=EDGE_LOOP ( 'NONE', ( #62956, #90823, #37268, #16820 ) ) ;
#43374=ORIENTED_EDGE ( 'NONE', *, *, #37292, .F. ) ;
#43375=B_SPLINE_CURVE_WITH_KNOTS ( 'NONE', 3,
 ( #69342, #45022, #98780, #21160 ),
 .UNSPECIFIED., .F., .F.,
 ( 4, 4 ),
 ( 0.000000000000000000, 1.000000000000000000 ),
 .UNSPECIFIED. ) ;
#43376=CARTESIAN_POINT ( 'NONE',  ( -30.64427850938830389, -23.56000036390796737, -1.497999999999532594 ) ) ;
#43380=CARTESIAN_POINT ( 'NONE',  ( -51.04357394935764347, -25.31543073408252553, 4.940877929217665887 ) ) ;
#43381=ORIENTED_EDGE ( 'NONE', *, *, #60048, .T. ) ;
#43382=CARTESIAN_POINT ( 'NONE',  ( -11.15089393765527959, -15.82809448842462885, 11.49999999999999645 ) ) ;
#43388=CARTESIAN_POINT ( 'NONE',  ( -30.47287095715007510, -23.47596703474403768, 11.44538124590455830 ) ) ;
#43390=CARTESIAN_POINT ( 'NONE',  ( -11.77723790057865116, -15.68276428244051779, -1.500000000000002220 ) ) ;
#43391=B_SPLINE_SURFACE_WITH_KNOTS ( 'NONE', 3, 3, ( 
 ( #92994, #46333, #77758, #55457 ),
 ( #15370, #32608, #47340, #55962 ),
 ( #157, #39713, #70672, #23470 ),
 ( #94000, #63583, #1669, #94506 ),
 ( #46840, #8272, #32101, #62070 ),
 ( #24987, #54451, #16374, #9770 ),
 ( #33111, #31602, #63075, #86891 ),
 ( #17384, #85385, #77264, #48346 ),
 ( #86395, #24489, #79276, #95006 ),
 ( #85894, #16878, #47841, #40724 ) ),
 .UNSPECIFIED., .F., .F., .F.,
 ( 4, 3, 3, 4 ),
 ( 4, 4 ),
 ( 0.0004766839783815776210, 0.1491231665100171133, 0.2234464077758348821, 0.2977696490416526509 ),
 ( 0.7995905709435781050, 0.8010797674005437630 ),
 .UNSPECIFIED. ) ;
#43393=ORIENTED_EDGE ( 'NONE', *, *, #45034, .T. ) ;
#43394=CARTESIAN_POINT ( 'NONE',  ( -18.53595284743415661, 10.95218985133829825, 11.49999999999998934 ) ) ;
#43395=CARTESIAN_POINT ( 'NONE',  ( -89.40841769935764205, -25.12049752546738191, 2.832404795212221327 ) ) ;
#43396=CARTESIAN_POINT ( 'NONE',  ( -80.46709582760330193, -25.30394759373683655, 4.967766255445141610 ) ) ;
#43397=FACE_OUTER_BOUND ( 'NONE', #74217, .T. ) ;
#43398=CARTESIAN_POINT ( 'NONE',  ( -99.52924129105133488, -25.27473359744577408, 3.929520238420538103 ) ) ;
#43399=CARTESIAN_POINT ( 'NONE',  ( -8.204236019480731557, -21.45505762417899831, -1.500000000000002220 ) ) ;
#43400=EDGE_CURVE ( 'NONE', #11305, #47218, #6685, .T. ) ;
#43404=CARTESIAN_POINT ( 'NONE',  ( -53.48693110046856702, -24.65952944569304250, 1.056160979905695463 ) ) ;
#43405=CARTESIAN_POINT ( 'NONE',  ( -18.82377384687745447, 7.257840063761761051, 11.49999999999999645 ) ) ;
#43407=CARTESIAN_POINT ( 'NONE',  ( -51.62287095715005592, -24.64965695001468404, 8.947790433994185832 ) ) ;
#43409=DIRECTION ( 'NONE',  ( -3.773278334453079618E-23, 0.9999999999976377785, 2.173523156925979975E-06 ) ) ;
#43411=CARTESIAN_POINT ( 'NONE',  ( -30.57287095715004099, -23.47593903913510260, -1.434903445928520149 ) ) ;
#43412=CARTESIAN_POINT ( 'NONE',  ( -19.08307359429613825, -5.530936995296134917, -1.500000000000002220 ) ) ;
#43415=CARTESIAN_POINT ( 'NONE',  ( 19.63295818312489871, -1.572306604260808260, -1.500000000000002220 ) ) ;
#43418=EDGE_CURVE ( 'NONE', #100230, #99338, #14039, .T. ) ;
#43419=B_SPLINE_CURVE_WITH_KNOTS ( 'NONE', 3,
 ( #58500, #89434, #12292, #74211 ),
 .UNSPECIFIED., .F., .F.,
 ( 4, 4 ),
 ( 0.000000000000000000, 9.999999999998897304E-05 ),
 .UNSPECIFIED. ) ;
#43422=CARTESIAN_POINT ( 'NONE',  ( -20.60850594246137035, -0.7621957659720622891, 11.49999999999999645 ) ) ;
#43423=CARTESIAN_POINT ( 'NONE',  ( -48.62287095715004881, -23.47596703998600276, 11.44779298504227505 ) ) ;
#43424=VECTOR ( 'NONE', #51321, 1000.000000000000114 ) ;
#43426=CARTESIAN_POINT ( 'NONE',  ( -9.675873947287982446, 20.46574270456686406, 11.49999999999999645 ) ) ;
#43431=B_SPLINE_CURVE_WITH_KNOTS ( 'NONE', 3,
 ( #92014, #13886, #92508, #61588 ),
 .UNSPECIFIED., .F., .F.,
 ( 4, 4 ),
 ( 0.000000000000000000, 9.999999999998897304E-05 ),
 .UNSPECIFIED. ) ;
#43432=CARTESIAN_POINT ( 'NONE',  ( -63.62745468079150868, -24.51314013834316796, 0.6176544820404160641 ) ) ;
#43433=DIRECTION ( 'NONE',  ( 0.000000000000000000, -0.9999999999976377785, -2.173523156925979128E-06 ) ) ;
#43435=ORIENTED_EDGE ( 'NONE', *, *, #96283, .T. ) ;
#43437=CARTESIAN_POINT ( 'NONE',  ( -99.42972581403923016, -25.19882830581870792, 6.611274056847894265 ) ) ;
#43438=CARTESIAN_POINT ( 'NONE',  ( 22.22072617242880455, -5.352622178732230118, -1.500000000000002220 ) ) ;
#43439=CARTESIAN_POINT ( 'NONE',  ( -74.62287095715007013, -24.34917612406838217, 0.1852690917426618733 ) ) ;
#43440=CARTESIAN_POINT ( 'NONE',  ( -4.019545577234938882, 21.20919285897865336, -1.500000000000002220 ) ) ;
#43444=CARTESIAN_POINT ( 'NONE',  ( 15.50834587592193259, -16.38432980155966590, 11.49999999999999645 ) ) ;
#43445=VERTEX_POINT ( 'NONE', #85056 ) ;
#43446=CARTESIAN_POINT ( 'NONE',  ( -70.13845683480205651, -25.24754246629652599, 4.855284388605379142 ) ) ;
#43447=CARTESIAN_POINT ( 'NONE',  ( 21.30657626330824783, 5.479626006175059239, -1.500000000000002220 ) ) ;
#43449=CARTESIAN_POINT ( 'NONE',  ( -128.6228709571500417, -29.50250786944525672, 11.44777988621622633 ) ) ;
#43450=VERTEX_POINT ( 'NONE', #60249 ) ;
#43453=ORIENTED_EDGE ( 'NONE', *, *, #2463, .F. ) ;
#43454=CARTESIAN_POINT ( 'NONE',  ( -53.52287095715006870, -29.50248528299804818, 1.056150453629033370 ) ) ;
#43455=EDGE_LOOP ( 'NONE', ( #51137, #52445, #66446, #78687 ) ) ;
#43456=ORIENTED_EDGE ( 'NONE', *, *, #85089, .T. ) ;
#43457=CARTESIAN_POINT ( 'NONE',  ( -65.52287095715006160, -24.99132157543083821, 2.256160258750667502 ) ) ;
#43458=FACE_OUTER_BOUND ( 'NONE', #79748, .T. ) ;
#43460=CARTESIAN_POINT ( 'NONE',  ( -20.22731604866883970, -2.807383831903240257, -1.500000000000002220 ) ) ;
#43462=CARTESIAN_POINT ( 'NONE',  ( -70.34543693012690824, -25.03284467579916495, 7.563174216508125269 ) ) ;
#43463=CARTESIAN_POINT ( 'NONE',  ( -30.64427850938830389, -23.56000036390796737, -1.497999999999532594 ) ) ;
#43464=CARTESIAN_POINT ( 'NONE',  ( -105.6347239592964087, -23.85016227208580730, -0.8807180028928328630 ) ) ;
#43465=CARTESIAN_POINT ( 'NONE',  ( -71.70841769935766763, -25.25855084132322048, 6.192981418235004476 ) ) ;
#43467=DIRECTION ( 'NONE',  ( 0.000000000000000000, 0.9999999999976377785, 2.173523156925979128E-06 ) ) ;
#43468=CARTESIAN_POINT ( 'NONE',  ( -27.85310238079214784, -24.63646064164220206, 8.249332086164569589 ) ) ;
#43469=ORIENTED_EDGE ( 'NONE', *, *, #69873, .T. ) ;
#43470=CARTESIAN_POINT ( 'NONE',  ( 10.19739565540945492, -18.13666118385682680, -1.500000000000002220 ) ) ;
#43472=CARTESIAN_POINT ( 'NONE',  ( -39.99567047530755559, -25.30560115809254285, 5.008336357703472075 ) ) ;
#43473=ORIENTED_EDGE ( 'NONE', *, *, #10457, .T. ) ;
#43474=EDGE_CURVE ( 'NONE', #49798, #61594, #98694, .T. ) ;
#43475=B_SPLINE_SURFACE_WITH_KNOTS ( 'NONE', 3, 3, ( 
 ( #16694, #54778, #23805, #979 ),
 ( #77085, #16193, #47161, #78081 ),
 ( #8592, #84203, #47663, #39541 ),
 ( #100410, #31931, #7586, #40040 ),
 ( #62900, #14693, #30921, #7086 ),
 ( #93823, #78579, #61891, #9086 ),
 ( #68987, #69494, #92814, #60889 ),
 ( #91817, #99910, #53777, #92318 ),
 ( #30422, #23295, #22789, #15195 ),
 ( #54281, #85207, #15697, #88225 ) ),
 .UNSPECIFIED., .F., .F., .F.,
 ( 4, 3, 3, 4 ),
 ( 4, 4 ),
 ( 0.7022005934544804928, 0.7765311282028795059, 0.8508616629512786300, 0.9995227324480767672 ),
 ( 0.8996025664823215084, 0.9011514415367618547 ),
 .UNSPECIFIED. ) ;
#43476=CARTESIAN_POINT ( 'NONE',  ( -51.52764846858840997, -25.25854370750454336, 6.187572764404343673 ) ) ;
#43477=CARTESIAN_POINT ( 'NONE',  ( -115.5228709571500190, -24.82558206586144678, 1.605769216559448598 ) ) ;
#43480=CARTESIAN_POINT ( 'NONE',  ( -114.6228709571500701, -24.51283580621365132, 0.6167428607019879161 ) ) ;
#43481=CARTESIAN_POINT ( 'NONE',  ( -76.52287095715007581, -23.47596703998600631, 11.44779298504228571 ) ) ;
#43482=DIRECTION ( 'NONE',  ( -0.000000000000000000, 2.173523156925979552E-06, -0.9999999999976378895 ) ) ;
#43483=CARTESIAN_POINT ( 'NONE',  ( -70.35895856474229504, -25.31201590484430142, 5.313173609717680712 ) ) ;
#43484=CARTESIAN_POINT ( 'NONE',  ( -14.46940225681120396, -16.66540133702554272, 11.49999999999999645 ) ) ;
#43486=CARTESIAN_POINT ( 'NONE',  ( -108.6235312761321552, -24.65952944569305316, 1.056160979905706121 ) ) ;
#43487=CARTESIAN_POINT ( 'NONE',  ( 1.383477600506065164, -22.57338898373578218, 11.49999999999998934 ) ) ;
#43489=EDGE_CURVE ( 'NONE', #92742, #41074, #84558, .T. ) ;
#43492=CARTESIAN_POINT ( 'NONE',  ( -57.52287095715003318, -24.66019654487198665, 8.947790411086121054 ) ) ;
#43493=ORIENTED_EDGE ( 'NONE', *, *, #48774, .T. ) ;
#43494=ORIENTED_EDGE ( 'NONE', *, *, #41905, .F. ) ;
#43495=EDGE_CURVE ( 'NONE', #90831, #73894, #17663, .T. ) ;
#43497=CARTESIAN_POINT ( 'NONE',  ( -57.50306194990486119, -24.15620529776628089, 10.23563542870660470 ) ) ;
#43498=EDGE_LOOP ( 'NONE', ( #78880, #84276, #89040, #70296 ) ) ;
#43500=CARTESIAN_POINT ( 'NONE',  ( -40.49165087243459737, -25.30507958278164793, 5.543942855563713579 ) ) ;
#43501=CARTESIAN_POINT ( 'NONE',  ( -10.38793682863964563, 19.71736701935523683, -1.500000000000002220 ) ) ;
#43502=PLANE ( 'NONE',  #21066 ) ;
#43503=EDGE_CURVE ( 'NONE', #89617, #84065, #43011, .T. ) ;
#43506=DIRECTION ( 'NONE',  ( -3.773278334453079618E-23, 0.9999999999976377785, 2.173523156925979975E-06 ) ) ;
#43507=CARTESIAN_POINT ( 'NONE',  ( -108.6228709571500417, -24.65952944569305316, 1.056160979905705011 ) ) ;
#43509=EDGE_CURVE ( 'NONE', #14950, #83990, #86564, .T. ) ;
#43510=CARTESIAN_POINT ( 'NONE',  ( -14.81708852449743929, -12.69844354874750181, -1.500000000000002220 ) ) ;
#43512=CARTESIAN_POINT ( 'NONE',  ( 0.5228555243449846124, 21.43159495547403282, 11.49999999999998934 ) ) ;
#43514=CARTESIAN_POINT ( 'NONE',  ( -107.5562042904834072, -23.48786465467241769, 11.44779295918253936 ) ) ;
#43516=CARTESIAN_POINT ( 'NONE',  ( 9.298244000614250382, 20.81247324795305431, -1.500000000000002220 ) ) ;
#43517=ADVANCED_FACE ( 'NONE', ( #46505 ), #17554, .T. ) ;
#43519=DIRECTION ( 'NONE',  ( 0.000000000000000000, -2.173523156925980399E-06, 0.9999999999976378895 ) ) ;
#43521=CARTESIAN_POINT ( 'NONE',  ( -8.876215969300202957, 17.89991547088461488, 11.49999999999999645 ) ) ;
#43522=CARTESIAN_POINT ( 'NONE',  ( -54.62287095715005592, -29.50247984919015209, -1.443849546365058689 ) ) ;
#43523=CARTESIAN_POINT ( 'NONE',  ( -91.62287095715004170, -24.66019654487199730, 8.947790411086124607 ) ) ;
#43524=CARTESIAN_POINT ( 'NONE',  ( -128.6228709571500417, -24.66019654487200441, 8.947790411086121054 ) ) ;
#43525=ORIENTED_EDGE ( 'NONE', *, *, #58977, .T. ) ;
#43526=CARTESIAN_POINT ( 'NONE',  ( -25.85421410313377066, -24.77680504942480866, 2.948317657866410535 ) ) ;
#43528=EDGE_CURVE ( 'NONE', #18101, #84750, #39402, .T. ) ;
#43529=CARTESIAN_POINT ( 'NONE',  ( 5.343276940429747768, -21.04383479052346217, 11.49999999999998934 ) ) ;
#43530=DIRECTION ( 'NONE',  ( -3.773278334453080206E-23, 0.9999999999976377785, 2.173523156925979975E-06 ) ) ;
#43531=CARTESIAN_POINT ( 'NONE',  ( -11.52932745282126703, -15.74164922852205173, -1.500000000000002220 ) ) ;
#43533=ADVANCED_FACE ( 'NONE', ( #94169 ), #99401, .T. ) ;
#43534=ORIENTED_EDGE ( 'NONE', *, *, #25845, .T. ) ;
#43537=CARTESIAN_POINT ( 'NONE',  ( -20.16212974941129588, 3.559051167911782887, 11.49999999999999645 ) ) ;
#43539=CARTESIAN_POINT ( 'NONE',  ( -39.62287095715007723, -23.95044443724991012, 10.65354141964650125 ) ) ;
#43542=CARTESIAN_POINT ( 'NONE',  ( -106.6228709571500275, -23.72773821059536559, 11.05748984161097681 ) ) ;
#43543=CARTESIAN_POINT ( 'NONE',  ( -78.62287095715005592, -24.33832256526968862, 0.1851278514119878704 ) ) ;
#43544=B_SPLINE_CURVE_WITH_KNOTS ( 'NONE', 3,
 ( #68075, #5171, #5666, #29000, #68572, #45239 ),
 .UNSPECIFIED., .F., .F.,
 ( 4, 2, 4 ),
 ( 1.570755371634111329E-05, 0.001396183895866089271, 0.002776660238015837747 ),
 .UNSPECIFIED. ) ;
#43545=CARTESIAN_POINT ( 'NONE',  ( -127.5228709571500616, -29.50250243563736774, 8.947779886222132717 ) ) ;
#43547=DIRECTION ( 'NONE',  ( -3.773278334453079030E-23, 0.9999999999976377785, 2.173523156925979128E-06 ) ) ;
#43549=CARTESIAN_POINT ( 'NONE',  ( -22.90524134523018773, 2.401388714834002069, 11.49999999999999645 ) ) ;
#43550=CARTESIAN_POINT ( 'NONE',  ( 6.015242202445381992, 21.98585358372262633, -1.500000000000002220 ) ) ;
#43551=CARTESIAN_POINT ( 'NONE',  ( -70.27422298781921484, -25.31517373419701755, 4.851635141314512900 ) ) ;
#43552=DIRECTION ( 'NONE',  ( 0.000000000000000000, 0.9999999999976377785, 2.173523156925979975E-06 ) ) ;
#43554=AXIS2_PLACEMENT_3D ( 'NONE', #75705, #14307, #60517 ) ;
#43555=CARTESIAN_POINT ( 'NONE',  ( -124.6228709571500559, -23.47593901973091235, -1.443836447538997536 ) ) ;
#43556=CARTESIAN_POINT ( 'NONE',  ( -110.5904913666769005, -24.40034930558991633, 0.3402023900116072364 ) ) ;
#43557=CARTESIAN_POINT ( 'NONE',  ( -5.132426408838210108, -21.30661980433056968, 11.49999999999998934 ) ) ;
#43559=CARTESIAN_POINT ( 'NONE',  ( -103.5228709571500474, -24.66019654487200441, 8.947790411086119278 ) ) ;
#43560=CARTESIAN_POINT ( 'NONE',  ( -120.6228709571500417, -23.47593901973091235, -1.443836447538997536 ) ) ;
#43563=VECTOR ( 'NONE', #91201, 1000.000000000000114 ) ;
#43564=CARTESIAN_POINT ( 'NONE',  ( 10.07161678670223637, 17.78519941539584792, -1.500000000000002220 ) ) ;
#43565=ORIENTED_EDGE ( 'NONE', *, *, #35868, .T. ) ;
#43566=ORIENTED_EDGE ( 'NONE', *, *, #63910, .F. ) ;
#43569=CARTESIAN_POINT ( 'NONE',  ( -3.733506833432379768, 22.73668382284982314, 11.49999999999998934 ) ) ;
#43570=DIRECTION ( 'NONE',  ( -3.773278334453079618E-23, 0.9999999999976377785, 2.173523156925979975E-06 ) ) ;
#43571=CARTESIAN_POINT ( 'NONE',  ( 19.26017855675105750, 6.235128648364509196, -1.500000000000002220 ) ) ;
#43572=VERTEX_POINT ( 'NONE', #27674 ) ;
#43573=CARTESIAN_POINT ( 'NONE',  ( -69.58953762381672448, -23.47596703998600276, 11.44779298504227505 ) ) ;
#43574=CARTESIAN_POINT ( 'NONE',  ( -48.52287095715006160, -23.48786465467241769, 11.44779295918255002 ) ) ;
#43575=CARTESIAN_POINT ( 'NONE',  ( -51.62287095715008434, -23.95044443724992433, 10.65354141964650125 ) ) ;
#43576=DIRECTION ( 'NONE',  ( 0.000000000000000000, -2.173523156925980399E-06, 0.9999999999976378895 ) ) ;
#43577=CARTESIAN_POINT ( 'NONE',  ( 3.659817510876246960, 21.07357064420920878, 11.49999999999999645 ) ) ;
#43578=ORIENTED_EDGE ( 'NONE', *, *, #8987, .T. ) ;
#43579=CARTESIAN_POINT ( 'NONE',  ( -55.52287095715006160, -24.62226745350438861, 0.9660975649728085202 ) ) ;
#43581=CARTESIAN_POINT ( 'NONE',  ( 20.56042274393015035, -8.519965759701490171, 11.49999999999998934 ) ) ;
#43582=CARTESIAN_POINT ( 'NONE',  ( -19.40337959798338119, 7.141409694766009508, -1.500000000000002220 ) ) ;
#43584=EDGE_LOOP ( 'NONE', ( #86987, #47685, #76147, #36190 ) ) ;
#43585=LINE ( 'NONE', #49214, #51803 ) ;
#43588=CARTESIAN_POINT ( 'NONE',  ( -129.5228709571500758, -24.64898659630529920, 1.056161002820834804 ) ) ;
#43591=CARTESIAN_POINT ( 'NONE',  ( 13.96602909953038640, 15.60522523583095200, -1.500000000000002220 ) ) ;
#43592=CARTESIAN_POINT ( 'NONE',  ( -12.46176837856299002, 18.05058065364367792, 11.49999999999999645 ) ) ;
#43594=LINE ( 'NONE', #28356, #4235 ) ;
#43595=CARTESIAN_POINT ( 'NONE',  ( -20.59131556071872282, -9.131246169528550283, -1.500000000000002220 ) ) ;
#43596=ADVANCED_FACE ( 'NONE', ( #50022 ), #73351, .T. ) ;
#43597=CARTESIAN_POINT ( 'NONE',  ( -7.049398010371669798, 19.71092172866906012, -1.500000000000002220 ) ) ;
#43598=PLANE ( 'NONE',  #2650 ) ;
#43599=ADVANCED_FACE ( 'NONE', ( #88575 ), #87568, .F. ) ;
#43600=CARTESIAN_POINT ( 'NONE',  ( -29.62287095715006302, -23.88397930277545456, 10.65359469698177541 ) ) ;
#43605=CARTESIAN_POINT ( 'NONE',  ( -66.53647785511840596, -24.65952944569304250, 1.056160979905692798 ) ) ;
#43606=CARTESIAN_POINT ( 'NONE',  ( -19.99255411920323056, 7.849732829375159149, -1.500000000000002220 ) ) ;
#43607=B_SPLINE_CURVE_WITH_KNOTS ( 'NONE', 3,
 ( #64771, #19053, #79452, #87573, #88081, #71858 ),
 .UNSPECIFIED., .F., .F.,
 ( 4, 2, 4 ),
 ( 6.384118696740187843E-06, 0.001386860460837440866, 0.002767336802978141459 ),
 .UNSPECIFIED. ) ;
#43608=CARTESIAN_POINT ( 'NONE',  ( -113.6228709571500559, -29.50250243563736774, 8.947779886222136270 ) ) ;
#43609=ORIENTED_EDGE ( 'NONE', *, *, #89330, .T. ) ;
#43610=CARTESIAN_POINT ( 'NONE',  ( -14.90395405082875335, 14.90835605916499418, 11.49999999999998934 ) ) ;
#43611=CARTESIAN_POINT ( 'NONE',  ( -60.55620429048339304, -25.00182538069145011, 7.747789668545098429 ) ) ;
#43613=PLANE ( 'NONE',  #65760 ) ;
#43615=CARTESIAN_POINT ( 'NONE',  ( -96.92287095715006728, -23.47596703998600631, 11.44779298504227860 ) ) ;
#43617=CARTESIAN_POINT ( 'NONE',  ( -129.5561478186664601, -23.48786465467241769, 11.44779295918253759 ) ) ;
#43618=CARTESIAN_POINT ( 'NONE',  ( -21.51168160490077952, -5.175097382202364926, -1.500000000000002220 ) ) ;
#43620=ADVANCED_FACE ( 'NONE', ( #81464 ), #62193, .T. ) ;
#43621=CARTESIAN_POINT ( 'NONE',  ( -108.9545715455115129, -25.27705962214097113, 4.170144839539424275 ) ) ;
#43622=CARTESIAN_POINT ( 'NONE',  ( -83.58953762381672448, -23.47593901973091235, -1.443836447539004642 ) ) ;
#43625=EDGE_CURVE ( 'NONE', #922, #26773, #99646, .T. ) ;
#43627=CARTESIAN_POINT ( 'NONE',  ( 7.684279652734260502, -19.92951104315265809, 11.49999999999998934 ) ) ;
#43628=CARTESIAN_POINT ( 'NONE',  ( -26.09993462008742426, -24.96876793076006251, 5.209353322998722113 ) ) ;
#43632=CARTESIAN_POINT ( 'NONE',  ( -15.40814491850785650, 16.58152744545821022, -1.500000000000002220 ) ) ;
#43633=ORIENTED_EDGE ( 'NONE', *, *, #90792, .F. ) ;
#43634=DIRECTION ( 'NONE',  ( -3.773278334444166432E-23, 1.000000000000000000, 0.000000000000000000 ) ) ;
#43635=CARTESIAN_POINT ( 'NONE',  ( -13.19171355488933983, -14.64934158388261665, 11.49999999999999645 ) ) ;
#43637=AXIS2_PLACEMENT_3D ( 'NONE', #19701, #18706, #80616 ) ;
#43638=B_SPLINE_CURVE_WITH_KNOTS ( 'NONE', 3,
 ( #85468, #738, #16961, #95092, #86475, #32184 ),
 .UNSPECIFIED., .F., .F.,
 ( 4, 2, 4 ),
 ( 0.000000000000000000, 0.001380901958385380088, 0.002761803916770760176 ),
 .UNSPECIFIED. ) ;
#43639=CARTESIAN_POINT ( 'NONE',  ( -119.5228709571501469, -24.34917612406838217, 0.1852690917426614570 ) ) ;
#43640=VERTEX_POINT ( 'NONE', #90558 ) ;
#43642=CARTESIAN_POINT ( 'NONE',  ( -29.02540380353726590, -24.60094009216138744, 2.175343837210148124 ) ) ;
#43644=CARTESIAN_POINT ( 'NONE',  ( -19.46174652491427182, -9.421329337880418819, 11.49999999999998934 ) ) ;
#43646=CARTESIAN_POINT ( 'NONE',  ( -4.359330469889163950, 18.88329184224734192, -1.500000000000002220 ) ) ;
#43648=CARTESIAN_POINT ( 'NONE',  ( -81.31915660432444781, -25.09456864601564519, 7.311523710026984091 ) ) ;
#43649=EDGE_CURVE ( 'NONE', #47809, #48068, #21530, .T. ) ;
#43650=CARTESIAN_POINT ( 'NONE',  ( 19.60560811685724403, 2.727087469661350738, -1.500000000000002220 ) ) ;
#43652=CARTESIAN_POINT ( 'NONE',  ( 18.08294815051442583, 9.098846914115775064, 11.49999999999999645 ) ) ;
#43654=B_SPLINE_CURVE_WITH_KNOTS ( 'NONE', 3,
 ( #48729, #24366, #16746, #2544, #34487, #71052 ),
 .UNSPECIFIED., .F., .F.,
 ( 4, 2, 4 ),
 ( 0.000000000000000000, 0.001380764517853248600, 0.002761529035706497201 ),
 .UNSPECIFIED. ) ;
#43655=EDGE_CURVE ( 'NONE', #65722, #21736, #5821, .T. ) ;
#43656=B_SPLINE_CURVE_WITH_KNOTS ( 'NONE', 3,
 ( #26540, #41264, #57504, #72718, #3216, #86429, #48882, #26028 ),
 .UNSPECIFIED., .F., .F.,
 ( 4, 2, 2, 4 ),
 ( -0.001224873891641426295, -0.0002244903592271089293, 0.0007758931731872084365, 0.002776660238015842518 ),
 .UNSPECIFIED. ) ;
#43659=B_SPLINE_SURFACE_WITH_KNOTS ( 'NONE', 3, 3, ( 
 ( #76490, #68893, #61301, #92227 ),
 ( #39451, #8501, #86120, #32840 ),
 ( #55692, #17106, #92718, #78999 ),
 ( #15105, #23206, #62810, #23712 ) ),
 .UNSPECIFIED., .F., .F., .F.,
 ( 4, 4 ),
 ( 4, 4 ),
 ( 0.3743040175512771239, 0.5066054860718446351 ),
 ( 0.8909579831155240992, 0.9113928628922632891 ),
 .UNSPECIFIED. ) ;
#43662=CARTESIAN_POINT ( 'NONE',  ( -71.52287095715007581, -23.48786465467241058, 11.44779295918254647 ) ) ;
#43665=CARTESIAN_POINT ( 'NONE',  ( 0.1258803491696451060, 20.03332480481931199, 11.49999999999998934 ) ) ;
#43667=ORIENTED_EDGE ( 'NONE', *, *, #69398, .F. ) ;
#43668=CARTESIAN_POINT ( 'NONE',  ( -102.5228709571500758, -24.64898659630367916, 1.056161002820829697 ) ) ;
#43669=CARTESIAN_POINT ( 'NONE',  ( -82.55620429048337883, -24.65952944569304606, 1.056160979905699460 ) ) ;
#43670=PLANE ( 'NONE',  #32224 ) ;
#43671=CARTESIAN_POINT ( 'NONE',  ( -113.5228709571500758, -24.33832256527049154, 0.1851278514138635367 ) ) ;
#43672=DIRECTION ( 'NONE',  ( -1.000000000000000000, -3.773278334444167608E-23, -8.201307810031802745E-29 ) ) ;
#43675=VECTOR ( 'NONE', #41966, 1000.000000000000114 ) ;
#43676=CARTESIAN_POINT ( 'NONE',  ( -18.23349369547262810, -8.965252873808195133, -1.500000000000002220 ) ) ;
#43678=CARTESIAN_POINT ( 'NONE',  ( 22.25235761598246143, -5.642936543268669780, 11.49999999999998934 ) ) ;
#43679=CARTESIAN_POINT ( 'NONE',  ( -65.52287095715006160, -23.47593901973090169, -1.443836447538996870 ) ) ;
#43683=CARTESIAN_POINT ( 'NONE',  ( -49.29494865489761679, -25.26264011037805801, 6.331091240045351398 ) ) ;
#43684=AXIS2_PLACEMENT_3D ( 'NONE', #4242, #28077, #88981 ) ;
#43686=CARTESIAN_POINT ( 'NONE',  ( -19.34623641613454836, -8.721557147202650739, 11.49999999999999645 ) ) ;
#43687=ORIENTED_EDGE ( 'NONE', *, *, #94550, .F. ) ;
#43688=VECTOR ( 'NONE', #69110, 1000.000000000000114 ) ;
#43690=CARTESIAN_POINT ( 'NONE',  ( -19.06252244145942498, 11.34236556261432405, -1.500000000000002220 ) ) ;
#43691=CARTESIAN_POINT ( 'NONE',  ( 16.39479758508079144, -12.47777281027006424, 11.49999999999998934 ) ) ;
#43692=AXIS2_PLACEMENT_3D ( 'NONE', #37852, #8395, #7388 ) ;
#43693=ORIENTED_EDGE ( 'NONE', *, *, #46692, .F. ) ;
#43694=ORIENTED_EDGE ( 'NONE', *, *, #43275, .F. ) ;
#43696=PLANE ( 'NONE',  #80991 ) ;
#43697=EDGE_LOOP ( 'NONE', ( #24400, #75612, #13747, #5585, #68895, #13478, #49937, #68038, #49170, #27481, #77984, #24149, #65825, #15256, #64738, #99524, #63912 ) ) ;
#43698=EDGE_CURVE ( 'NONE', #3121, #94573, #80560, .T. ) ;
#43699=VERTEX_POINT ( 'NONE', #44901 ) ;
#43700=ORIENTED_EDGE ( 'NONE', *, *, #45488, .F. ) ;
#43701=CARTESIAN_POINT ( 'NONE',  ( -111.7692696073655156, -25.28511524806629041, 4.136510707875227233 ) ) ;
#43702=CARTESIAN_POINT ( 'NONE',  ( -28.48666779331410481, -24.18640622799667028, 9.817618374534074377 ) ) ;
#43704=CARTESIAN_POINT ( 'NONE',  ( -4.307737697753418082, 20.33289072680551968, -1.500000000000002220 ) ) ;
#43705=CARTESIAN_POINT ( 'NONE',  ( -17.03913561245058261, -13.47071831616118942, 11.49999999999999645 ) ) ;
#43706=ORIENTED_EDGE ( 'NONE', *, *, #17773, .T. ) ;
#43707=ADVANCED_FACE ( 'NONE', ( #59626 ), #91297, .T. ) ;
#43708=CARTESIAN_POINT ( 'NONE',  ( -40.81961785418572930, -25.27806125868308484, 5.018035830796276464 ) ) ;
#43709=CARTESIAN_POINT ( 'NONE',  ( -34.55620429048339304, -23.47596703998600276, 11.44779298504227505 ) ) ;
#43710=CARTESIAN_POINT ( 'NONE',  ( -115.5568011907884483, -23.85016227208580730, -0.8807180028928282001 ) ) ;
#43711=CARTESIAN_POINT ( 'NONE',  ( -19.61019785865472542, -10.87575402790796453, -1.500000000000002220 ) ) ;
#43712=EDGE_CURVE ( 'NONE', #30369, #2649, #22522, .T. ) ;
#43713=CARTESIAN_POINT ( 'NONE',  ( -51.19090461678316473, -25.26334662982828405, 4.328065714047625079 ) ) ;
#43714=CARTESIAN_POINT ( 'NONE',  ( -65.49582848406727464, -24.52300882791528736, 0.6510814631126250474 ) ) ;
#43716=CARTESIAN_POINT ( 'NONE',  ( -71.20541289166536103, -25.31502801509702749, 4.885889949323629189 ) ) ;
#43719=ORIENTED_EDGE ( 'NONE', *, *, #89436, .F. ) ;
#43721=EDGE_CURVE ( 'NONE', #27242, #75066, #20538, .T. ) ;
#43722=ORIENTED_EDGE ( 'NONE', *, *, #45186, .T. ) ;
#43724=ORIENTED_EDGE ( 'NONE', *, *, #46793, .T. ) ;
#43725=CARTESIAN_POINT ( 'NONE',  ( 15.78869406909177897, -14.30566568001193950, -1.500000000000002220 ) ) ;
#43726=VERTEX_POINT ( 'NONE', #53013 ) ;
#43728=CARTESIAN_POINT ( 'NONE',  ( 17.34737195785526609, 13.27887811287985187, -1.500000000000002220 ) ) ;
#43730=CARTESIAN_POINT ( 'NONE',  ( 21.55457256799317278, 7.124301260279622738, -1.500000000000002220 ) ) ;
#43731=CARTESIAN_POINT ( 'NONE',  ( -112.6228709571500417, -24.65952944569304961, 1.056160979905702346 ) ) ;
#43733=CARTESIAN_POINT ( 'NONE',  ( 18.29167757401336303, -12.14499471347784798, -1.500000000000002220 ) ) ;
#43734=CARTESIAN_POINT ( 'NONE',  ( -87.63200249025274502, -24.15543982623908548, -0.2315651400026449980 ) ) ;
#43735=VERTEX_POINT ( 'NONE', #83943 ) ;
#43737=CARTESIAN_POINT ( 'NONE',  ( -40.05769137787242329, -25.29480120415430733, 5.514493779961309627 ) ) ;
#43738=PLANE ( 'NONE',  #86449 ) ;
#43739=EDGE_CURVE ( 'NONE', #96245, #89859, #76809, .T. ) ;
#43740=EDGE_LOOP ( 'NONE', ( #70241, #52822, #51570, #76520 ) ) ;
#43742=CARTESIAN_POINT ( 'NONE',  ( -130.5728709571501156, -24.75152770810921510, 1.363349870542273523 ) ) ;
#43743=CARTESIAN_POINT ( 'NONE',  ( -30.58711349467732532, -25.14094028198826436, 2.712351064733613537 ) ) ;
#43744=CARTESIAN_POINT ( 'NONE',  ( -18.64022381217131397, 10.26305532446727753, -1.500000000000002220 ) ) ;
#43745=FACE_OUTER_BOUND ( 'NONE', #24709, .T. ) ;
#43746=CARTESIAN_POINT ( 'NONE',  ( -26.42246413733907673, -24.97064590431050846, 3.141772897168136236 ) ) ;
#43748=FACE_OUTER_BOUND ( 'NONE', #83924, .T. ) ;
#43749=PLANE ( 'NONE',  #47542 ) ;
#43750=CARTESIAN_POINT ( 'NONE',  ( -90.62287095715004170, -24.99132157543084531, 2.256160258750667502 ) ) ;
#43752=CARTESIAN_POINT ( 'NONE',  ( -14.26233628608129855, 13.40890954296891024, 11.49999999999999645 ) ) ;
#43753=CARTESIAN_POINT ( 'NONE',  ( -58.62287095715005592, -24.51387760970723662, 9.387446482453421837 ) ) ;
#43755=CARTESIAN_POINT ( 'NONE',  ( -29.78631988578491629, -25.22684763970347888, 5.682124227929016058 ) ) ;
#43756=VERTEX_POINT ( 'NONE', #28664 ) ;
#43757=CARTESIAN_POINT ( 'NONE',  ( -117.5228709571500758, -23.47596703998600631, 11.44779298504227860 ) ) ;
#43758=CARTESIAN_POINT ( 'NONE',  ( -101.7073711143522416, -25.15401000799511522, 6.923429918029315289 ) ) ;
#43760=CARTESIAN_POINT ( 'NONE',  ( -27.06750426676058296, -24.63035931427080882, 8.145542352137882247 ) ) ;
#43761=CARTESIAN_POINT ( 'NONE',  ( -40.62287095715005592, -23.47596703998600276, 11.44779298504227505 ) ) ;
#43762=CARTESIAN_POINT ( 'NONE',  ( -11.91260469445801995, 15.66180005371307260, -1.500000000000002220 ) ) ;
#43763=AXIS2_PLACEMENT_3D ( 'NONE', #25081, #49447, #10871 ) ;
#43764=ORIENTED_EDGE ( 'NONE', *, *, #85741, .T. ) ;
#43766=B_SPLINE_CURVE_WITH_KNOTS ( 'NONE', 3,
 ( #21284, #68478, #14172, #5073, #98911, #99411, #45147, #76074, #36518, #36023, #37024, #13670, #6070, #6573, #37524, #82692 ),
 .UNSPECIFIED., .F., .F.,
 ( 4, 2, 2, 2, 2, 2, 2, 4 ),
 ( 0.000000000000000000, 0.0002294183186423333083, 0.0004588366372846666165, 0.0006882549559270000061, 0.0009176732745693332331, 0.001376509911854000012, 0.001605928230496330746, 0.001835346549138661262 ),
 .UNSPECIFIED. ) ;
#43769=AXIS2_PLACEMENT_3D ( 'NONE', #35991, #65978, #20256 ) ;
#43774=CARTESIAN_POINT ( 'NONE',  ( -45.62287095715004881, -24.15516710230293995, 10.28746687063725318 ) ) ;
#43775=CARTESIAN_POINT ( 'NONE',  ( -47.65343445879282314, -23.73766607897670866, -1.055555164236438914 ) ) ;
#43776=CARTESIAN_POINT ( 'NONE',  ( -62.62287095715004881, -23.47593901973091235, -1.443836447539007972 ) ) ;
#43778=DIRECTION ( 'NONE',  ( 0.000000000000000000, -2.173523156925980399E-06, 0.9999999999976378895 ) ) ;
#43779=CARTESIAN_POINT ( 'NONE',  ( -107.5890209867514642, -24.34968618360934300, 0.1864209137778969627 ) ) ;
#43780=CARTESIAN_POINT ( 'NONE',  ( 8.914523860536577970, -17.85282776015759154, -1.500000000000002220 ) ) ;
#43782=CARTESIAN_POINT ( 'NONE',  ( -37.52287095715008292, -23.48783264083359512, -1.443836473376374885 ) ) ;
#43783=CARTESIAN_POINT ( 'NONE',  ( -0.1141154322660206111, -21.57268605278876805, 10.89591856040522266 ) ) ;
#43784=ORIENTED_EDGE ( 'NONE', *, *, #87111, .T. ) ;
#43787=SHAPE_REPRESENTATION_RELATIONSHIP ( 'NONE' , 'NONE' ,  #37291, #30696 ) ;
#43788=LINE ( 'NONE', #61515, #83192 ) ;
#43790=CARTESIAN_POINT ( 'NONE',  ( -39.60860462615423927, -23.73766607897669800, -1.055555164236461341 ) ) ;
#43791=CARTESIAN_POINT ( 'NONE',  ( -64.52287095715007581, -23.96127896941631619, -0.6493128931038050222 ) ) ;
#43793=CARTESIAN_POINT ( 'NONE',  ( -51.19681519762799127, -25.26280088862281659, 4.857314488523241991 ) ) ;
#43795=CARTESIAN_POINT ( 'NONE',  ( -71.62287095715005592, -24.65952944569304606, 1.056160979905699016 ) ) ;
#43796=CARTESIAN_POINT ( 'NONE',  ( -127.5896358177784862, -24.34968618360935011, 0.1864209137778924386 ) ) ;
#43798=CARTESIAN_POINT ( 'NONE',  ( -0.9278407348523283193, 20.21260682001012654, 11.49999999999998934 ) ) ;
#43799=CARTESIAN_POINT ( 'NONE',  ( -105.6228709571500559, -23.48786465467241769, 11.44779295918253759 ) ) ;
#43801=CARTESIAN_POINT ( 'NONE',  ( -80.62287095715005592, -29.50247984919015209, -1.443849546365053582 ) ) ;
#43805=CARTESIAN_POINT ( 'NONE',  ( -19.29710791919172053, 5.528754708966634901, -1.500000000000002220 ) ) ;
#43806=CARTESIAN_POINT ( 'NONE',  ( 3.785439364192078937, -20.66625369722972749, 11.49999999999999645 ) ) ;
#43808=CARTESIAN_POINT ( 'NONE',  ( -32.52287095715004739, -23.96127896942119051, -0.6493128930941857169 ) ) ;
#43809=CARTESIAN_POINT ( 'NONE',  ( -13.58966412916292299, 17.40808962483262690, -1.500000000000002220 ) ) ;
#43811=DIRECTION ( 'NONE',  ( -3.773278334444168195E-23, 1.000000000000000000, 0.000000000000000000 ) ) ;
#43812=CARTESIAN_POINT ( 'NONE',  ( -34.58953762381672448, -23.47593901973091235, -1.443836447539013301 ) ) ;
#43813=DIRECTION ( 'NONE',  ( -1.000000000000000000, -3.773278334444167608E-23, -8.201307833595939069E-29 ) ) ;
#43816=CARTESIAN_POINT ( 'NONE',  ( -31.62935866127120832, -24.51314013834316086, 0.6176544820404139546 ) ) ;
#43817=EDGE_LOOP ( 'NONE', ( #56345, #36847, #17400, #14326 ) ) ;
#43818=B_SPLINE_CURVE_WITH_KNOTS ( 'NONE', 3,
 ( #84719, #22801, #37551, #70504, #45669, #77596 ),
 .UNSPECIFIED., .F., .F.,
 ( 4, 2, 4 ),
 ( 6.390294094803335792E-06, 0.001387608157368792720, 0.002768826020642782028 ),
 .UNSPECIFIED. ) ;
#43821=LINE ( 'NONE', #67173, #34046 ) ;
#43822=CARTESIAN_POINT ( 'NONE',  ( -76.56415044752040444, -23.48783264082477373, -1.443836473390089026 ) ) ;
#43823=CARTESIAN_POINT ( 'NONE',  ( 17.26003113218828489, 11.23261964116016642, -1.500000000000002220 ) ) ;
#43824=CARTESIAN_POINT ( 'NONE',  ( -14.35963886870962192, 16.04489112172382903, 11.49999999999999645 ) ) ;
#43826=CARTESIAN_POINT ( 'NONE',  ( -91.55809077531434070, -23.73766607897670156, -1.055555164236454235 ) ) ;
#43829=CARTESIAN_POINT ( 'NONE',  ( 21.44611857939883137, 6.294191480875499067, -1.500000000000002220 ) ) ;
#43833=CARTESIAN_POINT ( 'NONE',  ( -67.52287095715006160, -24.64965694238407323, 8.947790433994200043 ) ) ;
#43834=AXIS2_PLACEMENT_3D ( 'NONE', #15149, #51728, #35993 ) ;
#43836=ADVANCED_FACE ( 'NONE', ( #46381 ), #1215, .T. ) ;
#43838=CARTESIAN_POINT ( 'NONE',  ( 6.973883220674568229, 19.69035807221911938, 11.49999999999998934 ) ) ;
#43839=EDGE_CURVE ( 'NONE', #82501, #2671, #25036, .T. ) ;
#43841=B_SPLINE_CURVE_WITH_KNOTS ( 'NONE', 3,
 ( #38870, #54119, #1323, #69829, #86047, #70330 ),
 .UNSPECIFIED., .F., .F.,
 ( 4, 2, 4 ),
 ( 0.000000000000000000, 0.001380901958385393966, 0.002761803916770787931 ),
 .UNSPECIFIED. ) ;
#43842=DIRECTION ( 'NONE',  ( 1.000000000000000000, 3.773278334444167608E-23, 8.201307833595939069E-29 ) ) ;
#43846=CARTESIAN_POINT ( 'NONE',  ( -100.5450565129023062, -24.92592662359561473, 8.075495903018000021 ) ) ;
#43847=CARTESIAN_POINT ( 'NONE',  ( -13.65698368949537311, 16.12507722524849996, -1.500000000000002220 ) ) ;
#43848=ORIENTED_EDGE ( 'NONE', *, *, #2203, .T. ) ;
#43849=CARTESIAN_POINT ( 'NONE',  ( -117.6235066561394973, -24.65952944569305316, 1.056160979905706343 ) ) ;
#43850=CARTESIAN_POINT ( 'NONE',  ( -102.6228709571500701, -23.72773821059536559, 11.05748984161097503 ) ) ;
#43851=CARTESIAN_POINT ( 'NONE',  ( -98.52287095715006160, -29.50250786944525672, 11.44777988621623166 ) ) ;
#43853=CARTESIAN_POINT ( 'NONE',  ( -129.6228709571500417, -23.47596703998600631, 11.44779298504227683 ) ) ;
#43854=CARTESIAN_POINT ( 'NONE',  ( -12.78816955685674372, 17.57309652720472570, -1.500000000000002220 ) ) ;
#43855=CARTESIAN_POINT ( 'NONE',  ( -80.09821655188528666, -25.05200611405530609, 7.521384686245699669 ) ) ;
#43856=CARTESIAN_POINT ( 'NONE',  ( -3.941980378682776287, 21.93750326593198352, 11.49999999999999645 ) ) ;
#43859=LINE ( 'NONE', #21988, #6455 ) ;
#43860=CARTESIAN_POINT ( 'NONE',  ( -95.52287095715006160, -23.48786465467241769, 11.44779295918254114 ) ) ;
#43861=CARTESIAN_POINT ( 'NONE',  ( -88.88918693012689687, -25.22391110550272941, 6.409327647371936720 ) ) ;
#43862=ORIENTED_EDGE ( 'NONE', *, *, #58876, .T. ) ;
#43864=ORIENTED_EDGE ( 'NONE', *, *, #77232, .T. ) ;
#43866=CARTESIAN_POINT ( 'NONE',  ( -86.52287095715006160, -23.47596703998600631, 11.44779298504228393 ) ) ;
#43867=DIRECTION ( 'NONE',  ( 3.773278334444166432E-23, -1.000000000000000000, 0.000000000000000000 ) ) ;
#43868=LINE ( 'NONE', #35760, #98875 ) ;
#43869=CARTESIAN_POINT ( 'NONE',  ( -12.28997142660015740, 14.97987746540053422, -1.500000000000002220 ) ) ;
#43870=CARTESIAN_POINT ( 'NONE',  ( -36.62287095715005592, -24.66019654487199020, 8.947790411086138818 ) ) ;
#43871=ORIENTED_EDGE ( 'NONE', *, *, #80151, .T. ) ;
#43872=CARTESIAN_POINT ( 'NONE',  ( 11.07193147992585835, -15.93265361536492364, 11.49999999999999645 ) ) ;
#43874=B_SPLINE_CURVE_WITH_KNOTS ( 'NONE', 3,
 ( #89226, #80110, #4499, #35444, #20197, #12592, #72514, #74491 ),
 .UNSPECIFIED., .F., .F.,
 ( 4, 2, 2, 4 ),
 ( 6.384118678612269921E-06, 0.002007151183507259289, 0.003007534715921582943, 0.004007918248335905730 ),
 .UNSPECIFIED. ) ;
#43878=CARTESIAN_POINT ( 'NONE',  ( -102.6228709571500275, -24.34917612406837861, 0.1852690917426659811 ) ) ;
#43879=B_SPLINE_CURVE_WITH_KNOTS ( 'NONE', 3,
 ( #54514, #8330, #38777, #63642 ),
 .UNSPECIFIED., .F., .F.,
 ( 4, 4 ),
 ( 0.6402431064082777512, 0.6492495376803931739 ),
 .UNSPECIFIED. ) ;
#43880=CARTESIAN_POINT ( 'NONE',  ( -87.62287095715001328, -23.95044443724992078, 10.65354141964649415 ) ) ;
#43881=ADVANCED_FACE ( 'NONE', ( #17428 ), #39262, .T. ) ;
#43882=CARTESIAN_POINT ( 'NONE',  ( 19.52168601723349894, 1.684101417132040979, -1.500000000000002220 ) ) ;
#43885=CARTESIAN_POINT ( 'NONE',  ( -0.8629811567608781653, -21.54619324973139172, -1.500000000000002220 ) ) ;
#43886=DIRECTION ( 'NONE',  ( -3.773278334453079030E-23, 0.9999999999976377785, 2.173523156925979128E-06 ) ) ;
#43887=LINE ( 'NONE', #44895, #96701 ) ;
#43888=CARTESIAN_POINT ( 'NONE',  ( -62.52287095715006160, -24.64965694238406613, 8.947790433994201820 ) ) ;
#43889=AXIS2_PLACEMENT_3D ( 'NONE', #15871, #8269, #9260 ) ;
#43891=CARTESIAN_POINT ( 'NONE',  ( 3.792298468851710069, -22.70151372599487871, -1.500000000000002220 ) ) ;
#43892=EDGE_CURVE ( 'NONE', #50986, #50194, #34560, .T. ) ;
#43896=CARTESIAN_POINT ( 'NONE',  ( 9.271505649751263789, 17.87650053469100087, 11.49999999999999645 ) ) ;
#43897=CARTESIAN_POINT ( 'NONE',  ( -108.9585383990916796, -25.10927658323717537, 4.038060707102717473 ) ) ;
#43901=CARTESIAN_POINT ( 'NONE',  ( -110.6372435692922664, -25.18425590734490171, 3.331084500688020977 ) ) ;
#43902=CARTESIAN_POINT ( 'NONE',  ( -9.044204435542846809, 17.70297415775587169, -1.500000000000002220 ) ) ;
#43904=CARTESIAN_POINT ( 'NONE',  ( 13.37688099249405127, 14.58279310912311111, -1.500000000000002220 ) ) ;
#43905=CARTESIAN_POINT ( 'NONE',  ( -126.5558601108541836, -23.96169478059714208, 10.65365249895716637 ) ) ;
#43906=VECTOR ( 'NONE', #70824, 1000.000000000000114 ) ;
#43910=CARTESIAN_POINT ( 'NONE',  ( 6.115004186001010922, -19.73231167505474559, 11.49999999999999645 ) ) ;
#43912=EDGE_CURVE ( 'NONE', #4511, #2525, #34372, .T. ) ;
#43914=CARTESIAN_POINT ( 'NONE',  ( -63.52287095715004739, -23.47593901973090169, -1.443836447538996870 ) ) ;
#43915=CARTESIAN_POINT ( 'NONE',  ( 22.31954755298990278, 3.869410565987296380, 11.49999999999999645 ) ) ;
#43916=ORIENTED_EDGE ( 'NONE', *, *, #87470, .F. ) ;
#43920=B_SPLINE_CURVE_WITH_KNOTS ( 'NONE', 3,
 ( #40268, #7811, #14914, #71221 ),
 .UNSPECIFIED., .F., .F.,
 ( 4, 4 ),
 ( 0.000000000000000000, 9.999999999998897304E-05 ),
 .UNSPECIFIED. ) ;
#43922=EDGE_CURVE ( 'NONE', #40589, #73004, #46601, .T. ) ;
#43926=CARTESIAN_POINT ( 'NONE',  ( -21.74799678179195794, 7.114197580472080951, 11.49999999999998934 ) ) ;
#43928=CARTESIAN_POINT ( 'NONE',  ( 18.62697458635512859, 10.92912097662538251, -1.500000000000002220 ) ) ;
#43929=CARTESIAN_POINT ( 'NONE',  ( -113.5190789393543156, -23.96169478059713853, 10.65365249895717348 ) ) ;
#43930=CARTESIAN_POINT ( 'NONE',  ( -76.58953762381673869, -23.48786465467241058, 11.44779295918254469 ) ) ;
#43931=CARTESIAN_POINT ( 'NONE',  ( 1.525329354412473970, -22.51392980886878448, 11.49999999999999645 ) ) ;
#43933=CARTESIAN_POINT ( 'NONE',  ( -28.60206680416888858, -24.93038538096085688, 2.636305656040084600 ) ) ;
#43934=CARTESIAN_POINT ( 'NONE',  ( 16.16784302627978320, -14.93143893958281154, -1.500000000000002220 ) ) ;
#43938=PLANE ( 'NONE',  #99418 ) ;
#43939=CARTESIAN_POINT ( 'NONE',  ( -90.50597553108265458, -24.52399227489126687, 9.353111116836531735 ) ) ;
#43940=EDGE_LOOP ( 'NONE', ( #82474, #83482, #16544, #33455 ) ) ;
#43941=CARTESIAN_POINT ( 'NONE',  ( -29.52287095715006515, -23.65290397102212339, -1.053491145022395603 ) ) ;
#43943=ORIENTED_EDGE ( 'NONE', *, *, #4984, .T. ) ;
#43944=ADVANCED_FACE ( 'NONE', ( #9306 ), #70719, .F. ) ;
#43945=CARTESIAN_POINT ( 'NONE',  ( -65.52287095715007581, -24.14321612903117042, -0.2833117244521693445 ) ) ;
#43947=CARTESIAN_POINT ( 'NONE',  ( -36.60922706349395384, -23.73766607897670156, -1.055555164236459120 ) ) ;
#43948=CARTESIAN_POINT ( 'NONE',  ( -12.60687543931603471, -16.05746371069360379, -1.500000000000002220 ) ) ;
#43949=ORIENTED_EDGE ( 'NONE', *, *, #2028, .T. ) ;
#43952=CARTESIAN_POINT ( 'NONE',  ( -105.6251635957058710, -24.83618233451450408, 1.606449574219534826 ) ) ;
#43953=DIRECTION ( 'NONE',  ( 3.773278334444167608E-23, -1.000000000000000000, 0.000000000000000000 ) ) ;
#43956=CARTESIAN_POINT ( 'NONE',  ( -90.52287095715006160, -23.47593901973090524, -1.443836447538996426 ) ) ;
#43957=B_SPLINE_CURVE_WITH_KNOTS ( 'NONE', 3,
 ( #28097, #30076, #15346, #53435 ),
 .UNSPECIFIED., .F., .F.,
 ( 4, 4 ),
 ( 2.163172446012162672E-11, 0.001212141367717853692 ),
 .UNSPECIFIED. ) ;
#43958=CARTESIAN_POINT ( 'NONE',  ( 19.92439739378097840, -5.974006126113303949, 11.49999999999998934 ) ) ;
#43960=EDGE_CURVE ( 'NONE', #21736, #88376, #39197, .T. ) ;
#43961=VERTEX_POINT ( 'NONE', #50890 ) ;
#43963=ORIENTED_EDGE ( 'NONE', *, *, #60257, .F. ) ;
#43965=CARTESIAN_POINT ( 'NONE',  ( -28.62287095715004881, -23.57201582636175274, 11.05761041841422454 ) ) ;
#43966=LINE ( 'NONE', #38704, #6531 ) ;
#43969=DIRECTION ( 'NONE',  ( -0.000000000000000000, 2.173523156925979552E-06, -0.9999999999976378895 ) ) ;
#43971=DIRECTION ( 'NONE',  ( 0.000000000000000000, 0.9999999999976377785, 2.173523156925979128E-06 ) ) ;
#43972=CARTESIAN_POINT ( 'NONE',  ( -71.24017339641436308, -25.24515161739355307, 5.863458295308564772 ) ) ;
#43973=CARTESIAN_POINT ( 'NONE',  ( 9.107982344273736430, -20.20341329189913537, 11.49999999999999645 ) ) ;
#43974=VERTEX_POINT ( 'NONE', #18923 ) ;
#43975=EDGE_CURVE ( 'NONE', #20665, #22695, #98500, .T. ) ;
#43976=CARTESIAN_POINT ( 'NONE',  ( -108.5148114596531599, -24.34968618360934656, 0.1864209137778971292 ) ) ;
#43977=CARTESIAN_POINT ( 'NONE',  ( 21.37280783159109276, 7.349196219051140844, 11.49999999999998934 ) ) ;
#43978=EDGE_CURVE ( 'NONE', #38350, #91631, #42784, .T. ) ;
#43979=CARTESIAN_POINT ( 'NONE',  ( -115.6235241362618069, -25.00182538069147142, 7.747789668545041586 ) ) ;
#43983=CARTESIAN_POINT ( 'NONE',  ( -31.62287095715005236, -23.48786465467240347, 11.44779295918255180 ) ) ;
#43987=CARTESIAN_POINT ( 'NONE',  ( 5.670930919660429836, -21.52877996283707418, -1.500000000000002220 ) ) ;
#43988=CARTESIAN_POINT ( 'NONE',  ( -50.04527796557857755, -25.13941491172449005, 7.536031268920055481 ) ) ;
#43989=EDGE_LOOP ( 'NONE', ( #48318, #11968, #82494, #100415 ) ) ;
#43990=CARTESIAN_POINT ( 'NONE',  ( -78.58953762381672448, -23.47593901973091235, -1.443836447539004642 ) ) ;
#43991=CARTESIAN_POINT ( 'NONE',  ( -80.68466099729241137, -25.03432220282478937, 7.556350509324876619 ) ) ;
#43995=CARTESIAN_POINT ( 'NONE',  ( 16.96702763494397104, -9.608290155750392358, 11.49999999999998934 ) ) ;
#43996=CARTESIAN_POINT ( 'NONE',  ( -21.47443924280258187, -0.1944818460393343829, 11.49999999999998934 ) ) ;
#43998=PLANE ( 'NONE',  #68175 ) ;
#44000=CARTESIAN_POINT ( 'NONE',  ( -12.33899560737860313, 19.21699747222852395, -1.500000000000002220 ) ) ;
#44005=CARTESIAN_POINT ( 'NONE',  ( -106.5533739365583585, -24.15620529776629510, 10.23563542870659582 ) ) ;
#44006=CARTESIAN_POINT ( 'NONE',  ( -125.5562042904833930, -23.48783264082479150, -1.443836473390055941 ) ) ;
#44007=CARTESIAN_POINT ( 'NONE',  ( 12.75013301566243129, -15.34773647900153115, 11.49999999999999645 ) ) ;
#44009=CARTESIAN_POINT ( 'NONE',  ( -74.58799468583525538, -24.35071581493544102, 9.817618358456019934 ) ) ;
#44010=B_SPLINE_CURVE_WITH_KNOTS ( 'NONE', 3,
 ( #27571, #81847, #5219, #58522, #75710, #89463 ),
 .UNSPECIFIED., .F., .F.,
 ( 4, 2, 4 ),
 ( 1.570887131794638196E-05, 0.001396322306279758904, 0.002776935741241571502 ),
 .UNSPECIFIED. ) ;
#44011=FACE_OUTER_BOUND ( 'NONE', #96210, .T. ) ;
#44013=CARTESIAN_POINT ( 'NONE',  ( -27.33385579971651325, -24.59579688747963289, 1.660712602240671298 ) ) ;
#44014=CARTESIAN_POINT ( 'NONE',  ( -65.52287095715006160, -25.00182538069144655, 7.747789668545101982 ) ) ;
#44015=CARTESIAN_POINT ( 'NONE',  ( 15.89274262425319861, 14.76810421718133171, -1.500000000000002220 ) ) ;
#44016=CARTESIAN_POINT ( 'NONE',  ( -37.52287095715006870, -23.47593901973090524, -1.443836447538997314 ) ) ;
#44017=CARTESIAN_POINT ( 'NONE',  ( 19.54226456527178257, 0.3027743077981833730, -1.500000000000002220 ) ) ;
#44018=DIRECTION ( 'NONE',  ( -3.773278334453079618E-23, 0.9999999999976377785, 2.173523156925979975E-06 ) ) ;
#44019=ORIENTED_EDGE ( 'NONE', *, *, #36833, .T. ) ;
#44020=DIRECTION ( 'NONE',  ( -3.773278334444167608E-23, 1.000000000000000000, 0.000000000000000000 ) ) ;
#44021=CARTESIAN_POINT ( 'NONE',  ( -110.6228709571500559, -25.00158670708909625, 2.256160236439165967 ) ) ;
#44022=CARTESIAN_POINT ( 'NONE',  ( -2.888065500968368227, -20.30684875360264741, 11.49999999999999645 ) ) ;
#44023=LINE ( 'NONE', #26809, #19688 ) ;
#44025=B_SPLINE_CURVE_WITH_KNOTS ( 'NONE', 3,
 ( #53106, #14516, #38359, #45986 ),
 .UNSPECIFIED., .F., .F.,
 ( 4, 4 ),
 ( 0.000000000000000000, 9.999999999998897304E-05 ),
 .UNSPECIFIED. ) ;
#44026=DIRECTION ( 'NONE',  ( -0.000000000000000000, 2.173523156925979552E-06, -0.9999999999976378895 ) ) ;
#44027=B_SPLINE_CURVE_WITH_KNOTS ( 'NONE', 3,
 ( #54070, #47444, #48450, #40822, #32708, #260, #78372, #33211, #38819, #93597, #92601, #77868, #78868, #71785, #55564, #24090 ),
 .UNSPECIFIED., .F., .F.,
 ( 4, 2, 2, 2, 2, 2, 2, 4 ),
 ( 1.734723475976807094E-18, 0.0002333606573560949337, 0.0004667213147121881327, 0.0007000819720682813045, 0.0009334426294243745306, 0.001166803286780467757, 0.001400163944136560874, 0.001866885258848787876 ),
 .UNSPECIFIED. ) ;
#44028=EDGE_CURVE ( 'NONE', #48067, #55188, #40487, .T. ) ;
#44031=CARTESIAN_POINT ( 'NONE',  ( -106.6228709571500559, -24.64965695001469115, 8.947790433994176951 ) ) ;
#44035=CARTESIAN_POINT ( 'NONE',  ( -123.5228709571500900, -23.72773821059536914, 11.05748984161097148 ) ) ;
#44036=VERTEX_POINT ( 'NONE', #81333 ) ;
#44037=DIRECTION ( 'NONE',  ( 0.000000000000000000, 2.173523156925980399E-06, -0.9999999999976378895 ) ) ;
#44038=ADVANCED_FACE ( 'NONE', ( #3721 ), #18431, .T. ) ;
#44040=AXIS2_PLACEMENT_3D ( 'NONE', #90321, #13682, #67006 ) ;
#44041=CARTESIAN_POINT ( 'NONE',  ( 20.04565040668967413, 11.27863464804978477, 11.49999999999999645 ) ) ;
#44042=CARTESIAN_POINT ( 'NONE',  ( -12.29745307268338195, -19.16510367807413218, -1.500000000000002220 ) ) ;
#44045=CARTESIAN_POINT ( 'NONE',  ( -58.87764846858842560, -25.13069340115296058, 2.947789388436138580 ) ) ;
#44047=ADVANCED_FACE ( 'NONE', ( #65634 ), #11814, .T. ) ;
#44049=CARTESIAN_POINT ( 'NONE',  ( -69.58953762381671027, -24.64898659630528854, 1.056161002820825034 ) ) ;
#44050=CARTESIAN_POINT ( 'NONE',  ( 21.48171311866277122, -4.276277801222842179, 11.49999999999998934 ) ) ;
#44052=CARTESIAN_POINT ( 'NONE',  ( -34.55620429048339304, -24.66019654487199020, 8.947790411086138818 ) ) ;
#44053=CARTESIAN_POINT ( 'NONE',  ( -50.37830952628071657, -29.50249428492551829, 5.197779886230994073 ) ) ;
#44055=CARTESIAN_POINT ( 'NONE',  ( -58.58751465073510900, -24.34968618360933945, 0.1864209137778795045 ) ) ;
#44057=CARTESIAN_POINT ( 'NONE',  ( 13.31029742451639386, -15.53102932315203510, -1.500000000000002220 ) ) ;
#44058=VERTEX_POINT ( 'NONE', #12301 ) ;
#44061=ORIENTED_EDGE ( 'NONE', *, *, #42140, .F. ) ;
#44063=CARTESIAN_POINT ( 'NONE',  ( -7.156825135384894843, 21.90021990432103038, 11.49999999999998934 ) ) ;
#44064=PLANE ( 'NONE',  #32460 ) ;
#44065=CARTESIAN_POINT ( 'NONE',  ( 3.949161919925879172, -19.86910077469890723, -1.500000000000002220 ) ) ;
#44067=CARTESIAN_POINT ( 'NONE',  ( -77.62287095715005592, -29.50250243563736774, 8.947779886222141599 ) ) ;
#44069=B_SPLINE_CURVE_WITH_KNOTS ( 'NONE', 3,
 ( #78241, #56445, #1141, #63055 ),
 .UNSPECIFIED., .F., .F.,
 ( 4, 4 ),
 ( 0.000000000000000000, 9.999999999998900014E-05 ),
 .UNSPECIFIED. ) ;
#44070=B_SPLINE_CURVE_WITH_KNOTS ( 'NONE', 3,
 ( #24918, #40154, #71110, #1599, #31029, #61994 ),
 .UNSPECIFIED., .F., .F.,
 ( 4, 2, 4 ),
 ( 0.000000000000000000, 0.001380901958385381606, 0.002761803916770763211 ),
 .UNSPECIFIED. ) ;
#44071=CARTESIAN_POINT ( 'NONE',  ( -95.54721046836138498, -24.63355581998386157, 0.9682620441943944334 ) ) ;
#44072=CARTESIAN_POINT ( 'NONE',  ( -102.5228709571500758, -23.48786465467241769, 11.44779295918254114 ) ) ;
#44073=CARTESIAN_POINT ( 'NONE',  ( -0.4629837013611828866, -21.40787533109759977, 11.49999999999999645 ) ) ;
#44074=VERTEX_POINT ( 'NONE', #26039 ) ;
#44076=ORIENTED_EDGE ( 'NONE', *, *, #33647, .F. ) ;
#44077=CARTESIAN_POINT ( 'NONE',  ( 21.15429367616652101, -6.912965584596229895, 11.49999999999998934 ) ) ;
#44078=CARTESIAN_POINT ( 'NONE',  ( 7.508984785159893427, -19.29828013722326929, 11.49999999999998934 ) ) ;
#44080=ORIENTED_EDGE ( 'NONE', *, *, #30052, .F. ) ;
#44081=VECTOR ( 'NONE', #5917, 1000.000000000000227 ) ;
#44082=B_SPLINE_SURFACE_WITH_KNOTS ( 'NONE', 3, 1, ( 
 ( #38220, #45847 ),
 ( #21985, #76766 ),
 ( #90517, #82896 ),
 ( #22481, #29114 ),
 ( #75779, #13381 ),
 ( #13882, #22976 ),
 ( #44361, #91013 ),
 ( #83397, #7266 ),
 ( #69176, #75285 ),
 ( #53471, #60590 ),
 ( #100096, #44856 ),
 ( #6278, #36735 ),
 ( #77271, #99114 ),
 ( #53966, #67703 ),
 ( #37236, #92505 ) ),
 .UNSPECIFIED., .F., .F., .F.,
 ( 4, 1, 1, 1, 1, 1, 1, 1, 1, 1, 1, 1, 4 ),
 ( 2, 2 ),
 ( 0.000000000000000000, 0.09781818961471398788, 0.1997260534018261702, 0.3052763574779416844, 0.4158114905382919169, 0.4744722311435584650, 0.5372738797760969742, 0.6036574205596554332, 0.6742988630901268765, 0.7498344853162316470, 0.8285984767571028531, 0.9123777781577806500, 1.000000000000000000 ),
 ( 0.000000000000000000, 1.000000000000000000 ),
 .UNSPECIFIED. ) ;
#44083=EDGE_CURVE ( 'NONE', #24828, #76130, #22302, .T. ) ;
#44084=CARTESIAN_POINT ( 'NONE',  ( -28.67151963337447285, -23.33523189894360073, -1.443835813551990865 ) ) ;
#44087=ORIENTED_EDGE ( 'NONE', *, *, #54912, .T. ) ;
#44088=CARTESIAN_POINT ( 'NONE',  ( -12.67655569012464944, 16.65582705476778358, -1.500000000000002220 ) ) ;
#44089=CARTESIAN_POINT ( 'NONE',  ( 21.92589416912191069, -1.073809401359021143, 11.49999999999999645 ) ) ;
#44090=EDGE_CURVE ( 'NONE', #21186, #57878, #58635, .T. ) ;
#44091=CARTESIAN_POINT ( 'NONE',  ( -37.57004739008115024, -23.48786465467240347, 11.44779295918255357 ) ) ;
#44092=CARTESIAN_POINT ( 'NONE',  ( -6.671648801611133273, 21.52854475820963032, 11.49999999999998934 ) ) ;
#44093=CARTESIAN_POINT ( 'NONE',  ( -20.97355972163249049, 0.1317905507124840780, 11.49999999999998934 ) ) ;
#44096=CARTESIAN_POINT ( 'NONE',  ( -119.5539580184925796, -24.35071581493544457, 9.817618358456018157 ) ) ;
#44098=ORIENTED_EDGE ( 'NONE', *, *, #2457, .T. ) ;
#44099=EDGE_CURVE ( 'NONE', #55534, #294, #23557, .T. ) ;
#44100=ORIENTED_EDGE ( 'NONE', *, *, #50639, .F. ) ;
#44103=CARTESIAN_POINT ( 'NONE',  ( -128.6228709571500417, -23.73934037231758509, 11.05740245334327554 ) ) ;
#44104=CARTESIAN_POINT ( 'NONE',  ( -13.16228656746626591, 16.97819584282690286, -1.500000000000002220 ) ) ;
#44105=B_SPLINE_CURVE_WITH_KNOTS ( 'NONE', 3,
 ( #95114, #10374, #34225, #86996, #40331, #18983 ),
 .UNSPECIFIED., .F., .F.,
 ( 4, 2, 4 ),
 ( 0.000000000000000000, 0.001380901958385388545, 0.002761803916770777089 ),
 .UNSPECIFIED. ) ;
#44107=FACE_OUTER_BOUND ( 'NONE', #76366, .T. ) ;
#44108=ORIENTED_EDGE ( 'NONE', *, *, #45465, .T. ) ;
#44109=CARTESIAN_POINT ( 'NONE',  ( -13.65698368949537311, 16.12507722524849996, -1.500000000000002220 ) ) ;
#44113=CARTESIAN_POINT ( 'NONE',  ( -83.62359973981459405, -24.66019654487199375, 8.947790411086124607 ) ) ;
#44116=CARTESIAN_POINT ( 'NONE',  ( -18.93877658415168241, -11.43451605920036052, -1.500000000000002220 ) ) ;
#44118=B_SPLINE_CURVE_WITH_KNOTS ( 'NONE', 3,
 ( #48374, #79303, #73700, #4194, #13282, #89427, #6177, #44753, #36137, #19899 ),
 .UNSPECIFIED., .F., .F.,
 ( 4, 2, 2, 2, 4 ),
 ( 0.000000000000000000, 0.0002770619399313387575, 0.0005541238798626775151, 0.0008311858197940162184, 0.001108247759725355030 ),
 .UNSPECIFIED. ) ;
#44119=CARTESIAN_POINT ( 'NONE',  ( -109.7567281351150541, -25.28788469920083770, 5.668544159025581841 ) ) ;
#44124=CARTESIAN_POINT ( 'NONE',  ( -10.03281922573575002, -16.61734169602722488, 11.49999999999998934 ) ) ;
#44126=CARTESIAN_POINT ( 'NONE',  ( 16.79701800048795590, -13.18750964578662455, -1.500000000000002220 ) ) ;
#44128=CARTESIAN_POINT ( 'NONE',  ( -90.70839235003093393, -25.31768024997816013, 4.634761245912265792 ) ) ;
#44129=PLANE ( 'NONE',  #95700 ) ;
#44130=CARTESIAN_POINT ( 'NONE',  ( -100.4326965455115186, -25.27359974593377956, 3.293942923980552884 ) ) ;
#44131=B_SPLINE_CURVE_WITH_KNOTS ( 'NONE', 3,
 ( #36361, #28245, #19126, #81039, #65837, #5409 ),
 .UNSPECIFIED., .F., .F.,
 ( 4, 2, 4 ),
 ( 0.000000000000000000, 0.001380764517854763665, 0.002761529035709527329 ),
 .UNSPECIFIED. ) ;
#44132=CARTESIAN_POINT ( 'NONE',  ( 10.43192878459595185, 20.09917060401269850, -1.500000000000002220 ) ) ;
#44133=ORIENTED_EDGE ( 'NONE', *, *, #50464, .F. ) ;
#44135=CARTESIAN_POINT ( 'NONE',  ( -79.54658045552653789, -24.34968618360933945, 0.1864209137778814473 ) ) ;
#44136=CARTESIAN_POINT ( 'NONE',  ( -19.81728208556213389, 0.3677575464312098363, 11.49999999999999645 ) ) ;
#44138=CARTESIAN_POINT ( 'NONE',  ( -119.5228709571501611, -23.96127896941633040, -0.6493128931037963625 ) ) ;
#44140=CARTESIAN_POINT ( 'NONE',  ( -77.52287095715006160, -24.64898659630367916, 1.056161002820826145 ) ) ;
#44141=CARTESIAN_POINT ( 'NONE',  ( -28.67105337545913812, -24.60093948885277015, 1.897772093073314181 ) ) ;
#44142=CARTESIAN_POINT ( 'NONE',  ( -100.4799102492508780, -25.12268565644366447, 7.101073848355138551 ) ) ;
#44143=CARTESIAN_POINT ( 'NONE',  ( -21.62496174240652991, 0.2022338437372764308, -1.500000000000002220 ) ) ;
#44144=CARTESIAN_POINT ( 'NONE',  ( -49.10457154551148307, -25.10935380766095193, 3.999772607897646548 ) ) ;
#44145=CARTESIAN_POINT ( 'NONE',  ( -18.22047185089115828, 6.579378235550767506, -1.500000000000002220 ) ) ;
#44148=CARTESIAN_POINT ( 'NONE',  ( -17.91562471463183570, -8.470225615102204841, -1.500000000000002220 ) ) ;
#44150=CARTESIAN_POINT ( 'NONE',  ( -8.335131950130996614, 18.48905954037022781, 11.49999999999999645 ) ) ;
#44151=CARTESIAN_POINT ( 'NONE',  ( -54.58953762381672448, -24.66019654487199020, 8.947790411086131712 ) ) ;
#44154=EDGE_CURVE ( 'NONE', #47480, #53349, #5430, .T. ) ;
#44155=VERTEX_POINT ( 'NONE', #75205 ) ;
#44156=FACE_OUTER_BOUND ( 'NONE', #75012, .T. ) ;
#44161=CARTESIAN_POINT ( 'NONE',  ( -51.51966037441169277, -25.23394976452496152, 6.321922888134675844 ) ) ;
#44162=CARTESIAN_POINT ( 'NONE',  ( -13.75281105048956576, 14.62798779934380811, 11.49999999999998934 ) ) ;
#44164=CARTESIAN_POINT ( 'NONE',  ( -85.52287095715010423, -23.84047902841604127, -0.8780736468305390119 ) ) ;
#44165=ORIENTED_EDGE ( 'NONE', *, *, #76324, .T. ) ;
#44168=CARTESIAN_POINT ( 'NONE',  ( 21.82588152991271713, 6.770963248321698380, 11.49999999999999645 ) ) ;
#44169=CARTESIAN_POINT ( 'NONE',  ( -49.53524246831344868, -25.26258762038820294, 4.168640273188112921 ) ) ;
#44171=CARTESIAN_POINT ( 'NONE',  ( -86.62287095715008434, -23.94994826722515668, -0.6494450866351706431 ) ) ;
#44173=EDGE_CURVE ( 'NONE', #83609, #11601, #12799, .T. ) ;
#44175=PLANE ( 'NONE',  #2500 ) ;
#44176=CARTESIAN_POINT ( 'NONE',  ( 10.13505985054399083, -19.98934331558005439, 11.49999999999999645 ) ) ;
#44177=DIRECTION ( 'NONE',  ( -3.773278334453079618E-23, 0.9999999999976377785, 2.173523156925979975E-06 ) ) ;
#44178=ORIENTED_EDGE ( 'NONE', *, *, #66219, .T. ) ;
#44179=CARTESIAN_POINT ( 'NONE',  ( -5.548086588741434788, -19.59138962566686004, 11.49999999999998934 ) ) ;
#44181=EDGE_CURVE ( 'NONE', #72922, #7606, #76742, .T. ) ;
#44182=CARTESIAN_POINT ( 'NONE',  ( 17.95915693031428262, 14.28781372813260120, -1.500000000000002220 ) ) ;
#44183=CARTESIAN_POINT ( 'NONE',  ( -53.52287095715005449, -24.66019654487198665, 8.947790411086121054 ) ) ;
#44186=CARTESIAN_POINT ( 'NONE',  ( -77.53982194047173948, -24.66019654487200441, 8.947790411086108620 ) ) ;
#44187=VECTOR ( 'NONE', #81201, 1000.000000000000114 ) ;
#44188=EDGE_CURVE ( 'NONE', #55530, #2529, #93651, .T. ) ;
#44189=DIRECTION ( 'NONE',  ( -3.773278334453079030E-23, 0.9999999999976377785, 2.173523156925979128E-06 ) ) ;
#44190=CARTESIAN_POINT ( 'NONE',  ( -3.247986963444697395, 20.98610878802851332, 11.49999999999999645 ) ) ;
#44191=ORIENTED_EDGE ( 'NONE', *, *, #64581, .F. ) ;
#44193=EDGE_LOOP ( 'NONE', ( #28478, #3939, #61868, #99485 ) ) ;
#44194=CARTESIAN_POINT ( 'NONE',  ( -22.11311035156252558, 1.696007508605793301, -1.500000000000002220 ) ) ;
#44195=CARTESIAN_POINT ( 'NONE',  ( -20.25002411749221665, -3.895867502427604379, -1.500000000000002220 ) ) ;
#44196=EDGE_CURVE ( 'NONE', #420, #16998, #7696, .T. ) ;
#44197=B_SPLINE_CURVE_WITH_KNOTS ( 'NONE', 3,
 ( #78125, #47206, #16245, #70536, #29460, #38583 ),
 .UNSPECIFIED., .F., .F.,
 ( 4, 2, 4 ),
 ( 0.000000000000000000, 0.001380764517854762147, 0.002761529035709524293 ),
 .UNSPECIFIED. ) ;
#44200=VERTEX_POINT ( 'NONE', #23916 ) ;
#44203=ORIENTED_EDGE ( 'NONE', *, *, #63335, .F. ) ;
#44204=ORIENTED_EDGE ( 'NONE', *, *, #36146, .T. ) ;
#44205=EDGE_LOOP ( 'NONE', ( #80637, #90590, #1525, #74436 ) ) ;
#44206=CARTESIAN_POINT ( 'NONE',  ( -39.52287095715009002, -23.95044443724991368, 10.65354141964649592 ) ) ;
#44207=DIRECTION ( 'NONE',  ( -0.8760724843741984902, 0.000000000000000000, -0.4821794293853893798 ) ) ;
#44208=CARTESIAN_POINT ( 'NONE',  ( -119.5228709571500616, -23.48783264082477018, -1.443836473390082142 ) ) ;
#44209=CARTESIAN_POINT ( 'NONE',  ( 18.38559056850662543, 9.607341378227904016, -1.500000000000002220 ) ) ;
#44210=CARTESIAN_POINT ( 'NONE',  ( -1.994712787082457472, 21.64621699974126656, 11.49999999999999645 ) ) ;
#44211=EDGE_LOOP ( 'NONE', ( #86959, #95248, #5803, #92741 ) ) ;
#44212=CARTESIAN_POINT ( 'NONE',  ( -100.9357141943721530, -25.20148372820526816, 3.413620792782795732 ) ) ;
#44213=CARTESIAN_POINT ( 'NONE',  ( -100.5228709571500616, -29.50250786944525672, 11.44777988621623166 ) ) ;
#44214=CARTESIAN_POINT ( 'NONE',  ( -115.6323215094300991, -23.48783264082477018, -1.443836473390087916 ) ) ;
#44215=CARTESIAN_POINT ( 'NONE',  ( 9.841385673706204429, 20.17164819615926064, -1.500000000000002220 ) ) ;
#44216=EDGE_CURVE ( 'NONE', #23841, #54069, #30531, .T. ) ;
#44217=CARTESIAN_POINT ( 'NONE',  ( -40.01839366089613748, -25.30501058306510487, 5.509688048021296858 ) ) ;
#44218=ORIENTED_EDGE ( 'NONE', *, *, #65617, .T. ) ;
#44220=CARTESIAN_POINT ( 'NONE',  ( -51.69084450196597658, -25.24874092950897264, 3.825624438094035629 ) ) ;
#44221=B_SPLINE_SURFACE_WITH_KNOTS ( 'NONE', 3, 3, ( 
 ( #60480, #76165, #37118, #5174 ),
 ( #89418, #36129, #50864, #67099 ),
 ( #28508, #99003, #91396, #21873 ),
 ( #30500, #99501, #38111, #60971 ),
 ( #84786, #92896, #22372, #23886 ),
 ( #23373, #78164, #85799, #16279 ),
 ( #91896, #39618, #77665, #54859 ) ),
 .UNSPECIFIED., .F., .F., .F.,
 ( 4, 3, 4 ),
 ( 4, 4 ),
 ( 0.7945040050992243641, 0.8970133687736501216, 0.9995227324480757680 ),
 ( 0.3195752057335992657, 0.3207354674102795289 ),
 .UNSPECIFIED. ) ;
#44224=ADVANCED_FACE ( 'NONE', ( #78688 ), #583, .T. ) ;
#44225=PLANE ( 'NONE',  #26393 ) ;
#44226=VERTEX_POINT ( 'NONE', #15299 ) ;
#44227=CARTESIAN_POINT ( 'NONE',  ( 19.49461108348020133, 8.573440864381753457, -1.500000000000002220 ) ) ;
#44228=ORIENTED_EDGE ( 'NONE', *, *, #34085, .T. ) ;
#44231=CARTESIAN_POINT ( 'NONE',  ( -20.94189920129180038, 1.864940847883316488, 11.49999999999998934 ) ) ;
#44232=DIRECTION ( 'NONE',  ( 0.000000000000000000, -0.9999999999976377785, -2.173523156925979975E-06 ) ) ;
#44233=CARTESIAN_POINT ( 'NONE',  ( 21.16149768242404861, -8.233860041645145955, 11.49999999999998934 ) ) ;
#44234=PLANE ( 'NONE',  #42127 ) ;
#44236=CARTESIAN_POINT ( 'NONE',  ( 10.99670386783381737, -19.00842362925918749, -1.500000000000002220 ) ) ;
#44237=DIRECTION ( 'NONE',  ( -3.773278334453079030E-23, 0.9999999999976377785, 2.173523156925979128E-06 ) ) ;
#44240=ADVANCED_FACE ( 'NONE', ( #85312 ), #61498, .T. ) ;
#44242=ORIENTED_EDGE ( 'NONE', *, *, #74914, .F. ) ;
#44246=CARTESIAN_POINT ( 'NONE',  ( -30.61247030481453990, -24.47854930503728710, 0.5637492489085954572 ) ) ;
#44247=CARTESIAN_POINT ( 'NONE',  ( -16.96849063341007380, -12.82450338531451450, -1.500000000000002220 ) ) ;
#44248=CARTESIAN_POINT ( 'NONE',  ( -112.5918940264897543, -23.96119346886881729, -0.6495511937831842664 ) ) ;
#44250=CARTESIAN_POINT ( 'NONE',  ( -114.5228709571500332, -23.73907113217684284, -1.053371485781013916 ) ) ;
#44251=B_SPLINE_CURVE_WITH_KNOTS ( 'NONE', 3,
 ( #99579, #16356, #55439, #46316 ),
 .UNSPECIFIED., .F., .F.,
 ( 4, 4 ),
 ( 0.6992755142499577081, 0.7002762612907231787 ),
 .UNSPECIFIED. ) ;
#44252=CARTESIAN_POINT ( 'NONE',  ( -85.62287095715002749, -24.91570333823100114, 8.075032458375551059 ) ) ;
#44254=ORIENTED_EDGE ( 'NONE', *, *, #94892, .F. ) ;
#44255=CARTESIAN_POINT ( 'NONE',  ( -7.889300446747370188, -17.95381117360125955, 11.49999999999999645 ) ) ;
#44256=CARTESIAN_POINT ( 'NONE',  ( -78.52287095715007581, -23.96177878511308634, 10.65340807706329862 ) ) ;
#44257=CARTESIAN_POINT ( 'NONE',  ( -90.70649462243461869, -25.26877915520014639, 5.947789088310639904 ) ) ;
#44258=B_SPLINE_CURVE_WITH_KNOTS ( 'NONE', 3,
 ( #91954, #25329, #56306, #99548 ),
 .UNSPECIFIED., .F., .F.,
 ( 4, 4 ),
 ( 0.5308790877619156134, 0.5398855190340309251 ),
 .UNSPECIFIED. ) ;
#44259=EDGE_LOOP ( 'NONE', ( #5415, #41971, #61726, #66218 ) ) ;
#44260=CARTESIAN_POINT ( 'NONE',  ( -69.00197608513569492, -25.28274124714703319, 5.751830946319327786 ) ) ;
#44261=CARTESIAN_POINT ( 'NONE',  ( -99.38203303823797796, -25.31439660168539518, 5.782495694000596487 ) ) ;
#44262=CARTESIAN_POINT ( 'NONE',  ( -42.52287095715004739, -23.48783264083366973, -1.443836473376261642 ) ) ;
#44264=CARTESIAN_POINT ( 'NONE',  ( -89.49044893904931541, -25.11033443465437287, 2.832404802291436319 ) ) ;
#44265=CARTESIAN_POINT ( 'NONE',  ( -2.355416116969162754, -19.56741566493107598, 11.49999999999998934 ) ) ;
#44267=VERTEX_POINT ( 'NONE', #46261 ) ;
#44268=DIRECTION ( 'NONE',  ( -3.773278334453079618E-23, 0.9999999999976377785, 2.173523156925979975E-06 ) ) ;
#44272=EDGE_CURVE ( 'NONE', #72199, #69148, #29491, .T. ) ;
#44275=CARTESIAN_POINT ( 'NONE',  ( -103.6228709571500559, -23.48786465467241769, 11.44779295918254114 ) ) ;
#44276=CARTESIAN_POINT ( 'NONE',  ( -47.50045621308397159, -24.15543982623907127, -0.2315651400026536022 ) ) ;
#44277=CARTESIAN_POINT ( 'NONE',  ( -84.58953762381675290, -23.47596703998600631, 11.44779298504227683 ) ) ;
#44278=PLANE ( 'NONE',  #64764 ) ;
#44280=CARTESIAN_POINT ( 'NONE',  ( -69.79628282111092119, -25.31201622179200683, 5.458995709863208035 ) ) ;
#44282=CARTESIAN_POINT ( 'NONE',  ( -120.6228709571500417, -23.47593901973091235, -1.443836447538997536 ) ) ;
#44283=CARTESIAN_POINT ( 'NONE',  ( -18.23705311251027794, 8.147635122911419003, -1.500000000000002220 ) ) ;
#44285=CARTESIAN_POINT ( 'NONE',  ( -100.4381051993576506, -25.27532861597270042, 2.832404458683261961 ) ) ;
#44286=CARTESIAN_POINT ( 'NONE',  ( -0.05926229584106505049, -22.28280300962049054, 9.277709158646871401 ) ) ;
#44290=EDGE_CURVE ( 'NONE', #9907, #40297, #11353, .T. ) ;
#44291=CARTESIAN_POINT ( 'NONE',  ( -119.5222410164763147, -23.48783264082477373, -1.443836473390087916 ) ) ;
#44292=CARTESIAN_POINT ( 'NONE',  ( -80.58924316370918461, -24.52399227489127398, 9.353111116836524630 ) ) ;
#44293=CARTESIAN_POINT ( 'NONE',  ( -127.4335858270658832, -25.30062225142111032, 5.394419286057580365 ) ) ;
#44294=CARTESIAN_POINT ( 'NONE',  ( -81.54694949955771222, -24.34968618360933945, 0.1864209137778954084 ) ) ;
#44295=CARTESIAN_POINT ( 'NONE',  ( -28.13975365244298388, -24.60093900632847053, 1.675771093763900099 ) ) ;
#44297=ORIENTED_EDGE ( 'NONE', *, *, #80045, .F. ) ;
#44300=B_SPLINE_CURVE_WITH_KNOTS ( 'NONE', 3,
 ( #62983, #2573, #16280, #17792 ),
 .UNSPECIFIED., .F., .F.,
 ( 4, 4 ),
 ( 0.3590215203896768847, 0.3600222674304420223 ),
 .UNSPECIFIED. ) ;
#44301=CARTESIAN_POINT ( 'NONE',  ( -127.5892768804099404, -24.65952944569305316, 1.056160979905708341 ) ) ;
#44302=EDGE_LOOP ( 'NONE', ( #20770, #4515, #22220, #7988 ) ) ;
#44303=B_SPLINE_CURVE_WITH_KNOTS ( 'NONE', 3,
 ( #87350, #47296, #95467, #78223 ),
 .UNSPECIFIED., .F., .F.,
 ( 4, 4 ),
 ( 0.000000000000000000, 9.999999999998897304E-05 ),
 .UNSPECIFIED. ) ;
#44304=CARTESIAN_POINT ( 'NONE',  ( -19.72078065558051208, -4.686549088087978099, 11.49999999999998934 ) ) ;
#44305=CARTESIAN_POINT ( 'NONE',  ( -105.5562042904833788, -24.99156044556202971, 7.747789690856173195 ) ) ;
#44308=LINE ( 'NONE', #35690, #5472 ) ;
#44310=CARTESIAN_POINT ( 'NONE',  ( -116.5228709571500616, -24.64965694238575011, 8.947790433994191162 ) ) ;
#44311=FACE_OUTER_BOUND ( 'NONE', #70395, .T. ) ;
#44312=CARTESIAN_POINT ( 'NONE',  ( 7.746586651691365510, 18.53313339873204058, -1.500000000000002220 ) ) ;
#44313=VECTOR ( 'NONE', #64149, 1000.000000000000114 ) ;
#44314=CARTESIAN_POINT ( 'NONE',  ( 20.78037738254806399, 3.014218216234254566, 11.49999999999999645 ) ) ;
#44315=CARTESIAN_POINT ( 'NONE',  ( -29.24636659181000198, -25.21267509515801564, 4.940287023516041209 ) ) ;
#44316=CARTESIAN_POINT ( 'NONE',  ( -111.6228709571500559, -24.64965695001468404, 8.947790433994176951 ) ) ;
#44317=CARTESIAN_POINT ( 'NONE',  ( 2.303347834742990763, 21.97011321758780866, 11.49999999999998934 ) ) ;
#44318=CARTESIAN_POINT ( 'NONE',  ( 18.14102482237423075, -9.550406459077080967, -1.500000000000002220 ) ) ;
#44319=CARTESIAN_POINT ( 'NONE',  ( -39.44687923781921057, -25.27805912342874706, 4.188173683520872714 ) ) ;
#44322=ORIENTED_EDGE ( 'NONE', *, *, #81373, .F. ) ;
#44323=CARTESIAN_POINT ( 'NONE',  ( -100.2744028882005409, -25.12156721190337905, 2.838270228797207917 ) ) ;
#44324=CARTESIAN_POINT ( 'NONE',  ( -130.5728709571500588, -23.47596703998600631, 11.44779298504227860 ) ) ;
#44325=VERTEX_POINT ( 'NONE', #55386 ) ;
#44326=ORIENTED_EDGE ( 'NONE', *, *, #71496, .T. ) ;
#44328=CARTESIAN_POINT ( 'NONE',  ( -81.22287095715006444, -23.47596703998600631, 11.44779298504227860 ) ) ;
#44329=CARTESIAN_POINT ( 'NONE',  ( -76.58463740794132946, -24.51314013834316441, 0.6176544820404190617 ) ) ;
#44330=CARTESIAN_POINT ( 'NONE',  ( -19.32567751138619982, -7.045664331180771178, -1.500000000000002220 ) ) ;
#44331=CARTESIAN_POINT ( 'NONE',  ( -18.53595284743415661, 10.95218985133829825, 11.49999999999999645 ) ) ;
#44333=FACE_OUTER_BOUND ( 'NONE', #63811, .T. ) ;
#44335=CARTESIAN_POINT ( 'NONE',  ( 14.50327815619135308, -17.01817589256642194, -1.500000000000002220 ) ) ;
#44337=CARTESIAN_POINT ( 'NONE',  ( -93.52287095715007581, -23.72747288104470798, -1.053458166803226348 ) ) ;
#44341=CARTESIAN_POINT ( 'NONE',  ( -49.58207262147149663, -24.51419770103158413, 9.386484678747189392 ) ) ;
#44343=CARTESIAN_POINT ( 'NONE',  ( 20.83135763335140922, 1.668377004047274959, -1.500000000000002220 ) ) ;
#44344=ORIENTED_EDGE ( 'NONE', *, *, #16689, .T. ) ;
#44345=EDGE_CURVE ( 'NONE', #13092, #51806, #44070, .T. ) ;
#44346=LINE ( 'NONE', #152, #29555 ) ;
#44350=CARTESIAN_POINT ( 'NONE',  ( -100.5221651912381589, -23.48786465467241413, 11.44779295918254469 ) ) ;
#44351=CARTESIAN_POINT ( 'NONE',  ( -5.075574613727041218, 20.51645923614106337, -1.500000000000002220 ) ) ;
#44353=EDGE_LOOP ( 'NONE', ( #76364, #27377, #35961, #20607 ) ) ;
#44354=CARTESIAN_POINT ( 'NONE',  ( -112.5228709571500616, -23.47596703998600631, 11.44779298504228038 ) ) ;
#44355=CARTESIAN_POINT ( 'NONE',  ( -49.04309943529236904, -25.29535962531968707, 5.511470466757466546 ) ) ;
#44356=CARTESIAN_POINT ( 'NONE',  ( -110.3346797185884327, -25.18492896333868813, 3.293943116708551777 ) ) ;
#44358=CARTESIAN_POINT ( 'NONE',  ( -28.52287095715005094, -23.31182002239687989, -1.443836447538998202 ) ) ;
#44359=CARTESIAN_POINT ( 'NONE',  ( -33.52287095715006160, -23.47593901973090169, -1.443836447538997314 ) ) ;
#44360=CARTESIAN_POINT ( 'NONE',  ( -9.430186865587145917, -19.61854929170128869, -1.500000000000002220 ) ) ;
#44361=CARTESIAN_POINT ( 'NONE',  ( -71.56719770743626441, -25.31639610870687918, 5.535760714805260996 ) ) ;
#44362=CARTESIAN_POINT ( 'NONE',  ( 21.15698459081360383, -7.064864530413820454, 11.49999999999999645 ) ) ;
#44363=EDGE_LOOP ( 'NONE', ( #14339, #51405, #52865, #68693 ) ) ;
#44366=CARTESIAN_POINT ( 'NONE',  ( -100.9228709571500673, -23.47593901973090169, -1.443836447538996870 ) ) ;
#44367=ORIENTED_EDGE ( 'NONE', *, *, #97536, .T. ) ;
#44372=PLANE ( 'NONE',  #18712 ) ;
#44374=CARTESIAN_POINT ( 'NONE',  ( -15.38109395195050233, 11.78095549196778258, 11.49999999999998934 ) ) ;
#44376=ORIENTED_EDGE ( 'NONE', *, *, #91231, .F. ) ;
#44377=CARTESIAN_POINT ( 'NONE',  ( -5.798782886354239885, 18.49141925852020663, 11.49999999999999645 ) ) ;
#44378=FACE_OUTER_BOUND ( 'NONE', #19348, .T. ) ;
#44384=CARTESIAN_POINT ( 'NONE',  ( -87.62287095715002749, -24.50321055353804667, 9.387540953477525818 ) ) ;
#44386=CARTESIAN_POINT ( 'NONE',  ( -19.57149217635686966, 1.386223266712492297, 11.49999999999998934 ) ) ;
#44387=B_SPLINE_CURVE_WITH_KNOTS ( 'NONE', 3,
 ( #84359, #99568, #84860, #30071 ),
 .UNSPECIFIED., .F., .F.,
 ( 4, 4 ),
 ( 0.000000000000000000, 0.0001000000000000028644 ),
 .UNSPECIFIED. ) ;
#44389=CARTESIAN_POINT ( 'NONE',  ( -46.53038060754152383, -24.65952944569304606, 1.056160979905696351 ) ) ;
#44391=CARTESIAN_POINT ( 'NONE',  ( 19.98928912078053699, -8.061568661392884749, 11.49999999999998934 ) ) ;
#44392=CARTESIAN_POINT ( 'NONE',  ( -85.62287095715005592, -23.47596703998600631, 11.44779298504227860 ) ) ;
#44395=DIRECTION ( 'NONE',  ( -3.773278334453079618E-23, 0.9999999999976377785, 2.173523156925979975E-06 ) ) ;
#44396=CARTESIAN_POINT ( 'NONE',  ( 17.43399715339889511, -14.94103553264482720, -1.500000000000002220 ) ) ;
#44399=CARTESIAN_POINT ( 'NONE',  ( -49.62369267386219462, -24.65952944569304606, 1.056160979905696129 ) ) ;
#44400=CARTESIAN_POINT ( 'NONE',  ( 10.61947033613929214, 17.11087026910869469, 11.49999999999999645 ) ) ;
#44401=CARTESIAN_POINT ( 'NONE',  ( -109.6441887128288784, -25.28814102335254788, 2.986266316960244804 ) ) ;
#44403=EDGE_CURVE ( 'NONE', #21992, #25724, #36880, .T. ) ;
#44404=CARTESIAN_POINT ( 'NONE',  ( -104.6228709571500559, -24.65952944569304961, 1.056160979905701236 ) ) ;
#44405=PLANE ( 'NONE',  #94209 ) ;
#44406=B_SPLINE_CURVE_WITH_KNOTS ( 'NONE', 3,
 ( #53287, #67028, #84218, #97936, #20815, #54794 ),
 .UNSPECIFIED., .F., .F.,
 ( 4, 2, 4 ),
 ( 1.570887131794638196E-05, 0.001396322306279763458, 0.002776935741241580609 ),
 .UNSPECIFIED. ) ;
#44407=CARTESIAN_POINT ( 'NONE',  ( -111.1213521864704035, -25.29779229951232011, 3.637108192089848480 ) ) ;
#44408=CARTESIAN_POINT ( 'NONE',  ( -11.18921147948170614, -16.41150865552512883, 11.49999999999998934 ) ) ;
#44409=EDGE_CURVE ( 'NONE', #2532, #73037, #2936, .T. ) ;
#44410=LINE ( 'NONE', #75334, #30135 ) ;
#44411=CARTESIAN_POINT ( 'NONE',  ( 17.16143643543069075, 9.858047367376444825, -1.500000000000002220 ) ) ;
#44412=CARTESIAN_POINT ( 'NONE',  ( -126.5562100481780448, -23.73791477778912551, 11.05961554403169878 ) ) ;
#44413=EDGE_CURVE ( 'NONE', #64035, #13507, #12615, .T. ) ;
#44414=EDGE_CURVE ( 'NONE', #68323, #73714, #62229, .T. ) ;
#44417=CARTESIAN_POINT ( 'NONE',  ( -17.26476610439243231, 11.37957233835482818, 11.49999999999999645 ) ) ;
#44420=DIRECTION ( 'NONE',  ( 1.000000000000000000, 3.773278334444166432E-23, 8.201307841325785021E-29 ) ) ;
#44421=PLANE ( 'NONE',  #58730 ) ;
#44422=CARTESIAN_POINT ( 'NONE',  ( -22.67762270672801250, 1.536325718666671225, 11.49999999999999645 ) ) ;
#44423=ORIENTED_EDGE ( 'NONE', *, *, #15306, .F. ) ;
#44424=CARTESIAN_POINT ( 'NONE',  ( -91.62287095715004170, -23.47593901973091235, -1.443836447539002865 ) ) ;
#44430=ORIENTED_EDGE ( 'NONE', *, *, #49978, .F. ) ;
#44431=CARTESIAN_POINT ( 'NONE',  ( -98.62287095715007013, -23.47596703998600631, 11.44779298504227860 ) ) ;
#44432=CARTESIAN_POINT ( 'NONE',  ( -20.40978113611479827, 10.34812579263477872, 11.49999999999998934 ) ) ;
#44434=CARTESIAN_POINT ( 'NONE',  ( 14.33184905138074683, -16.10332302735202958, -1.500000000000002220 ) ) ;
#44435=CARTESIAN_POINT ( 'NONE',  ( -123.5538550107125673, -24.65952944569305316, 1.056160979905706343 ) ) ;
#44437=CARTESIAN_POINT ( 'NONE',  ( -22.39070119279581306, -2.479732019442284496, 11.49999999999999645 ) ) ;
#44439=DIRECTION ( 'NONE',  ( -3.773278334444167608E-23, 1.000000000000000000, 0.000000000000000000 ) ) ;
#44440=CARTESIAN_POINT ( 'NONE',  ( 3.689792033372774060, 21.67897595795444587, -1.500000000000002220 ) ) ;
#44441=CARTESIAN_POINT ( 'NONE',  ( -105.5995568635892425, -23.48786465467241769, 11.44779295918254114 ) ) ;
#44442=CARTESIAN_POINT ( 'NONE',  ( -41.77018777319382536, -25.29087217084345340, 3.672889645907745138 ) ) ;
#44443=EDGE_LOOP ( 'NONE', ( #24826, #96348, #66232, #16012 ) ) ;
#44444=DIRECTION ( 'NONE',  ( -1.000000000000000000, -3.773278334444166432E-23, -8.201307841325785021E-29 ) ) ;
#44445=CARTESIAN_POINT ( 'NONE',  ( -90.54280662865561169, -24.83644354573578994, 8.397322867130100121 ) ) ;
#44446=ORIENTED_EDGE ( 'NONE', *, *, #74519, .F. ) ;
#44447=CARTESIAN_POINT ( 'NONE',  ( -29.52287095715006515, -24.26482661340494573, 0.1850815758097280328 ) ) ;
#44449=ORIENTED_EDGE ( 'NONE', *, *, #60102, .F. ) ;
#44450=CARTESIAN_POINT ( 'NONE',  ( -49.34347621332902634, -25.28835214115807872, 5.818256392113962505 ) ) ;
#44453=CARTESIAN_POINT ( 'NONE',  ( 13.86372479123709311, 15.02075200336711092, -1.500000000000002220 ) ) ;
#44454=AXIS2_PLACEMENT_3D ( 'NONE', #18232, #8620, #72528 ) ;
#44457=CARTESIAN_POINT ( 'NONE',  ( -30.59128290392954952, -24.93418366566757882, 8.369064737642425200 ) ) ;
#44458=B_SPLINE_CURVE_WITH_KNOTS ( 'NONE', 3,
 ( #90827, #37040, #68492, #75584 ),
 .UNSPECIFIED., .F., .F.,
 ( 4, 4 ),
 ( 0.000000000000000000, 0.0001000000000000028644 ),
 .UNSPECIFIED. ) ;
#44460=B_SPLINE_CURVE_WITH_KNOTS ( 'NONE', 3,
 ( #90302, #97416, #20772, #36508 ),
 .UNSPECIFIED., .F., .F.,
 ( 4, 4 ),
 ( 0.000000000000000000, 9.999999999998897304E-05 ),
 .UNSPECIFIED. ) ;
#44462=CARTESIAN_POINT ( 'NONE',  ( -47.55620429048338593, -23.48786465467241058, 11.44779295918254292 ) ) ;
#44463=ORIENTED_EDGE ( 'NONE', *, *, #10468, .T. ) ;
#44464=PLANE ( 'NONE',  #54909 ) ;
#44465=CARTESIAN_POINT ( 'NONE',  ( -101.5228709571500900, -23.48783264082477018, -1.443836473390087249 ) ) ;
#44466=CARTESIAN_POINT ( 'NONE',  ( 2.040502595053849788, 20.68626321094233944, 11.49999999999998934 ) ) ;
#44467=EDGE_LOOP ( 'NONE', ( #17624, #47036, #97737, #60322 ) ) ;
#44468=EDGE_CURVE ( 'NONE', #90388, #32133, #55033, .T. ) ;
#44470=VERTEX_POINT ( 'NONE', #82586 ) ;
#44472=EDGE_LOOP ( 'NONE', ( #28329, #74147, #83510, #27117 ) ) ;
#44473=ORIENTED_EDGE ( 'NONE', *, *, #70538, .T. ) ;
#44474=DIRECTION ( 'NONE',  ( -3.773278334444167608E-23, 1.000000000000000000, 0.000000000000000000 ) ) ;
#44475=CARTESIAN_POINT ( 'NONE',  ( -119.1722388760374258, -25.27126041720326199, 4.079010001960293508 ) ) ;
#44478=CARTESIAN_POINT ( 'NONE',  ( -17.14978611337857473, 13.99085498846200437, 11.49999999999999645 ) ) ;
#44479=ORIENTED_EDGE ( 'NONE', *, *, #41584, .T. ) ;
#44481=CARTESIAN_POINT ( 'NONE',  ( -20.48750165597241590, 9.616757810196778777, 11.49999999999998934 ) ) ;
#44482=B_SPLINE_CURVE_WITH_KNOTS ( 'NONE', 3,
 ( #10716, #73613, #72622, #86826 ),
 .UNSPECIFIED., .F., .F.,
 ( 4, 4 ),
 ( 2.081668171172168513E-17, 0.0001000000000000097897 ),
 .UNSPECIFIED. ) ;
#44483=CARTESIAN_POINT ( 'NONE',  ( -99.29935056655477865, -25.30468847391853870, 5.154975380674369667 ) ) ;
#44484=ORIENTED_EDGE ( 'NONE', *, *, #36268, .T. ) ;
#44485=VERTEX_POINT ( 'NONE', #95939 ) ;
#44486=VECTOR ( 'NONE', #75314, 1000.000000000000114 ) ;
#44489=CARTESIAN_POINT ( 'NONE',  ( -20.11654390397962544, -0.4351469013266864860, -1.500000000000002220 ) ) ;
#44491=LINE ( 'NONE', #75415, #44081 ) ;
#44492=ORIENTED_EDGE ( 'NONE', *, *, #62512, .T. ) ;
#44494=B_SPLINE_CURVE_WITH_KNOTS ( 'NONE', 3,
 ( #4402, #35353, #58681, #89629, #20110, #51073 ),
 .UNSPECIFIED., .F., .F.,
 ( 4, 2, 4 ),
 ( 0.000000000000000000, 0.001380764517854767134, 0.002761529035709534268 ),
 .UNSPECIFIED. ) ;
#44495=CARTESIAN_POINT ( 'NONE',  ( 21.15429367616652101, -6.912965584596229895, -1.500000000000002220 ) ) ;
#44496=B_SPLINE_CURVE_WITH_KNOTS ( 'NONE', 3,
 ( #31051, #83846, #31559, #8230, #76223, #38670 ),
 .UNSPECIFIED., .F., .F.,
 ( 4, 2, 4 ),
 ( 0.000000000000000000, 0.001380764517853252937, 0.002761529035706505875 ),
 .UNSPECIFIED. ) ;
#44499=CARTESIAN_POINT ( 'NONE',  ( -119.5228709571500758, -23.48786465467241769, 11.44779295918253759 ) ) ;
#44500=CARTESIAN_POINT ( 'NONE',  ( -31.24388727629348494, -29.50250091417111520, 8.247779886223803203 ) ) ;
#44501=DIRECTION ( 'NONE',  ( -3.773278334444167608E-23, 1.000000000000000000, 0.000000000000000000 ) ) ;
#44502=CARTESIAN_POINT ( 'NONE',  ( -73.58953762381673869, -24.64965694238407323, 8.947790433994656567 ) ) ;
#44503=CARTESIAN_POINT ( 'NONE',  ( -18.23695082634099407, 6.967386181637144738, -1.500000000000002220 ) ) ;
#44504=CARTESIAN_POINT ( 'NONE',  ( -16.68621059303058018, 13.52761613308161870, 11.49999999999998934 ) ) ;
#44505=CARTESIAN_POINT ( 'NONE',  ( -25.53214279450137170, -24.92775365639140972, 4.846046591611402832 ) ) ;
#44506=CARTESIAN_POINT ( 'NONE',  ( -56.62287095715005592, -24.64898659630528499, 1.056161002820822592 ) ) ;
#44507=CARTESIAN_POINT ( 'NONE',  ( -122.6228709571500417, -29.50250243563736774, 8.947779886222134493 ) ) ;
#44508=CARTESIAN_POINT ( 'NONE',  ( -21.19308438721250099, -8.479022899233653376, -1.500000000000002220 ) ) ;
#44512=CARTESIAN_POINT ( 'NONE',  ( -108.5228709571500758, -23.48783264083353473, -1.443836473376470586 ) ) ;
#44513=CARTESIAN_POINT ( 'NONE',  ( -15.85412420263326538, -12.13584807887712458, 11.49999999999999645 ) ) ;
#44514=CARTESIAN_POINT ( 'NONE',  ( -63.52287095715006160, -29.50248528299804818, 1.056150453629034924 ) ) ;
#44515=CARTESIAN_POINT ( 'NONE',  ( -57.52287095715005449, -24.64898659630528854, 1.056161002820822592 ) ) ;
#44516=DIRECTION ( 'NONE',  ( 0.000000000000000000, 2.173523156925980399E-06, -0.9999999999976378895 ) ) ;
#44519=CARTESIAN_POINT ( 'NONE',  ( -83.52287095715006160, -23.73934037231757088, 11.05740245334328442 ) ) ;
#44522=CARTESIAN_POINT ( 'NONE',  ( 1.329761939549756855, 21.69843865049760367, 11.49999999999998934 ) ) ;
#44523=CARTESIAN_POINT ( 'NONE',  ( -37.62287095715005592, -23.47593901973091235, -1.443836447539011525 ) ) ;
#44524=CARTESIAN_POINT ( 'NONE',  ( -9.542874777335924819, 17.09510996321218101, -1.500000000000002220 ) ) ;
#44525=CARTESIAN_POINT ( 'NONE',  ( -80.52287095715006160, -23.48786465467241769, 11.44779295918254469 ) ) ;
#44526=EDGE_LOOP ( 'NONE', ( #80284, #6428, #51702, #13773 ) ) ;
#44529=CARTESIAN_POINT ( 'NONE',  ( -75.62287095715005592, -29.50250243563736774, 8.947779886222141599 ) ) ;
#44531=CARTESIAN_POINT ( 'NONE',  ( 1.819314030819549233, -20.42850443921780013, 11.49999999999999645 ) ) ;
#44532=CARTESIAN_POINT ( 'NONE',  ( -47.52287095715005449, -24.51387760970724017, 9.387446482453409402 ) ) ;
#44534=CARTESIAN_POINT ( 'NONE',  ( -53.92287095715006018, -23.47596703998600276, 11.44779298504227860 ) ) ;
#44536=CARTESIAN_POINT ( 'NONE',  ( -30.47959251904011424, -23.47596703649177385, 11.44618536770630968 ) ) ;
#44537=CARTESIAN_POINT ( 'NONE',  ( -40.16027052433451416, -25.28892429773494044, 3.329282795352901836 ) ) ;
#44539=ADVANCED_FACE ( 'NONE', ( #17310 ), #48275, .F. ) ;
#44540=CARTESIAN_POINT ( 'NONE',  ( -61.62287095715004881, -24.64898659630528854, 1.056161002820822592 ) ) ;
#44542=CARTESIAN_POINT ( 'NONE',  ( -119.6228709571500417, -24.65952944569304961, 1.056160979905704789 ) ) ;
#44543=CARTESIAN_POINT ( 'NONE',  ( -6.685540227124203483, -22.02754839873749404, 11.49999999999999645 ) ) ;
#44544=CARTESIAN_POINT ( 'NONE',  ( -2.506051680461856890, -22.62920675306992280, -1.500000000000002220 ) ) ;
#44545=CARTESIAN_POINT ( 'NONE',  ( -115.6228709571500559, -24.99132157543166954, 2.256160258750667502 ) ) ;
#44546=CARTESIAN_POINT ( 'NONE',  ( -45.52287095715006160, -23.47596703998600631, 11.44779298504229104 ) ) ;
#44547=CARTESIAN_POINT ( 'NONE',  ( -120.5228709571500900, -24.14406661686758682, 10.28769366194082657 ) ) ;
#44549=CARTESIAN_POINT ( 'NONE',  ( -40.52287095715007581, -24.83620972994592435, 8.398175272781369216 ) ) ;
#44550=CARTESIAN_POINT ( 'NONE',  ( -110.6272474294926269, -24.52300882791530512, 0.6510814631126382590 ) ) ;
#44551=CARTESIAN_POINT ( 'NONE',  ( 18.42579859434530931, 11.83097890990371148, 11.49999999999998934 ) ) ;
#44553=CARTESIAN_POINT ( 'NONE',  ( -87.58566455517073734, -24.51419770103156281, 9.386484678747175181 ) ) ;
#44555=CARTESIAN_POINT ( 'NONE',  ( -28.62287095715007013, -23.79486920467889988, -0.6496301281144789552 ) ) ;
#44556=CARTESIAN_POINT ( 'NONE',  ( -94.62287095715004170, -24.35013146730204525, 9.818937971375104823 ) ) ;
#44557=CARTESIAN_POINT ( 'NONE',  ( -86.62287095715009855, -23.95044443724992789, 10.65354141964649592 ) ) ;
#44558=ORIENTED_EDGE ( 'NONE', *, *, #75789, .T. ) ;
#44559=CARTESIAN_POINT ( 'NONE',  ( 5.028806042385554953, -19.83023610923392610, 11.49999999999998934 ) ) ;
#44560=ORIENTED_EDGE ( 'NONE', *, *, #48002, .F. ) ;
#44562=VERTEX_POINT ( 'NONE', #56402 ) ;
#44565=CARTESIAN_POINT ( 'NONE',  ( -19.45891602060003578, 12.32625358835968576, 11.49999999999998934 ) ) ;
#44566=CARTESIAN_POINT ( 'NONE',  ( -61.55369709315033333, -23.96119346886880308, -0.6495511937832122440 ) ) ;
#44567=CARTESIAN_POINT ( 'NONE',  ( 4.066846734877469949, -19.79409818376439389, -1.500000000000002220 ) ) ;
#44572=CARTESIAN_POINT ( 'NONE',  ( -95.54871114897673579, -24.52300882791530512, 0.6510814631126408125 ) ) ;
#44573=CARTESIAN_POINT ( 'NONE',  ( -99.55766099210418929, -23.73791477778911840, 11.05961554403170588 ) ) ;
#44574=CARTESIAN_POINT ( 'NONE',  ( -13.24026558610970916, 16.85365899302435722, 11.49999999999999645 ) ) ;
#44575=EDGE_LOOP ( 'NONE', ( #97855, #9544, #37657, #75408 ) ) ;
#44576=CARTESIAN_POINT ( 'NONE',  ( -77.52287095715007581, -23.48783264082476308, -1.443836473390091912 ) ) ;
#44577=B_SPLINE_CURVE_WITH_KNOTS ( 'NONE', 3,
 ( #15221, #39566, #49569, #34337, #26219, #92837 ),
 .UNSPECIFIED., .F., .F.,
 ( 4, 2, 4 ),
 ( 0.000000000000000000, 0.001380764517854766050, 0.002761529035709532100 ),
 .UNSPECIFIED. ) ;
#44578=CARTESIAN_POINT ( 'NONE',  ( -41.62371455830013645, -24.65952944569304606, 1.056160979905696351 ) ) ;
#44580=CARTESIAN_POINT ( 'NONE',  ( -20.69558417703438025, 1.077208295497980250, -1.500000000000002220 ) ) ;
#44582=ORIENTED_EDGE ( 'NONE', *, *, #50600, .F. ) ;
#44583=EDGE_CURVE ( 'NONE', #33754, #28964, #15562, .T. ) ;
#44585=ORIENTED_EDGE ( 'NONE', *, *, #97162, .T. ) ;
#44587=ORIENTED_EDGE ( 'NONE', *, *, #16893, .T. ) ;
#44588=CARTESIAN_POINT ( 'NONE',  ( -2.639205680565387624, -20.84613592336672028, -1.500000000000002220 ) ) ;
#44589=CARTESIAN_POINT ( 'NONE',  ( 6.372119535971386917, -21.01724095701019479, 11.49999999999999645 ) ) ;
#44590=AXIS2_PLACEMENT_3D ( 'NONE', #9890, #87016, #40841 ) ;
#44591=CARTESIAN_POINT ( 'NONE',  ( -73.60710170687688958, -23.48786465467241058, 11.44779295918254824 ) ) ;
#44592=CARTESIAN_POINT ( 'NONE',  ( -17.96456891314058879, -13.58578184957126034, 11.49999999999998934 ) ) ;
#44594=CARTESIAN_POINT ( 'NONE',  ( -11.48448384864204996, -17.54081393385053644, 11.49999999999998934 ) ) ;
#44599=ORIENTED_EDGE ( 'NONE', *, *, #60450, .T. ) ;
#44601=CARTESIAN_POINT ( 'NONE',  ( -66.63617382715514736, -24.15543982623906771, -0.2315651400026688400 ) ) ;
#44603=CARTESIAN_POINT ( 'NONE',  ( -10.41973078503355588, 18.78793304046337198, -1.500000000000002220 ) ) ;
#44604=DIRECTION ( 'NONE',  ( -0.000000000000000000, 2.173523156925979552E-06, -0.9999999999976378895 ) ) ;
#44606=CARTESIAN_POINT ( 'NONE',  ( -9.620199658202244208, 18.81650055922726494, -1.500000000000002220 ) ) ;
#44607=CARTESIAN_POINT ( 'NONE',  ( -52.62287095715006302, -23.72773821059535493, 11.05748984161097503 ) ) ;
#44608=CARTESIAN_POINT ( 'NONE',  ( -64.64155661987921064, -23.96119346886879953, -0.6495511937832134652 ) ) ;
#44610=CARTESIAN_POINT ( 'NONE',  ( -83.56309760437380874, -23.48786465467241058, 11.44779295918254469 ) ) ;
#44612=CARTESIAN_POINT ( 'NONE',  ( -69.55126625704998844, -25.16221347177320666, 3.076695569926833684 ) ) ;
#44613=CARTESIAN_POINT ( 'NONE',  ( 1.014068502963303864, -22.09113584270698993, -1.500000000000002220 ) ) ;
#44614=CARTESIAN_POINT ( 'NONE',  ( -81.49976054116859814, -24.66019654487198665, 8.947790411086131712 ) ) ;
#44615=VERTEX_POINT ( 'NONE', #75956 ) ;
#44616=CARTESIAN_POINT ( 'NONE',  ( -56.52287095715006870, -23.47596703998600631, 11.44779298504228926 ) ) ;
#44617=PLANE ( 'NONE',  #37864 ) ;
#44619=EDGE_CURVE ( 'NONE', #54649, #93563, #387, .T. ) ;
#44620=EDGE_CURVE ( 'NONE', #72780, #21913, #6958, .T. ) ;
#44621=CARTESIAN_POINT ( 'NONE',  ( -100.6412016622194727, -23.48783264082476663, -1.443836473390090358 ) ) ;
#44622=CARTESIAN_POINT ( 'NONE',  ( -15.52061920455031618, -11.66286593722069931, 11.49999999999998934 ) ) ;
#44624=CARTESIAN_POINT ( 'NONE',  ( -7.638042729800005759, 19.97414216180626667, -1.500000000000002220 ) ) ;
#44625=CARTESIAN_POINT ( 'NONE',  ( -61.62287095715004881, -29.50250786944525672, 11.44777988621623876 ) ) ;
#44626=PLANE ( 'NONE',  #96575 ) ;
#44629=CARTESIAN_POINT ( 'NONE',  ( -22.62345309801473547, -0.4825844212548152656, -1.500000000000002220 ) ) ;
#44630=ORIENTED_EDGE ( 'NONE', *, *, #92459, .F. ) ;
#44632=CARTESIAN_POINT ( 'NONE',  ( -102.5228709571500758, -24.64965694238407323, 8.947790433994194714 ) ) ;
#44633=CARTESIAN_POINT ( 'NONE',  ( 1.028332004353105233, 19.75660188889424518, 11.49999999999999645 ) ) ;
#44636=CARTESIAN_POINT ( 'NONE',  ( -35.58953762381673158, -25.00158670708909270, 2.256160236439166411 ) ) ;
#44637=EDGE_CURVE ( 'NONE', #60030, #39828, #97265, .T. ) ;
#44639=CARTESIAN_POINT ( 'NONE',  ( -78.62287095715005592, -29.50247984919015209, -1.443849546365053582 ) ) ;
#44640=FACE_OUTER_BOUND ( 'NONE', #28872, .T. ) ;
#44641=CARTESIAN_POINT ( 'NONE',  ( 4.348677445931066643, 21.19853102677161871, -1.500000000000002220 ) ) ;
#44642=CARTESIAN_POINT ( 'NONE',  ( -49.73634623139758304, -25.10935161048781339, 2.988891661266243283 ) ) ;
#44643=CARTESIAN_POINT ( 'NONE',  ( -1.608633542659107629, -19.34071428503001755, -1.500000000000002220 ) ) ;
#44644=DIRECTION ( 'NONE',  ( 0.000000000000000000, -2.173523156925980399E-06, 0.9999999999976378895 ) ) ;
#44645=DIRECTION ( 'NONE',  ( -3.773278334453079618E-23, 0.9999999999976377785, 2.173523156925979975E-06 ) ) ;
#44646=CARTESIAN_POINT ( 'NONE',  ( 18.24360591643979035, -7.691401616277519615, -1.500000000000002220 ) ) ;
#44648=CARTESIAN_POINT ( 'NONE',  ( -15.70679263237263434, -12.88635299011707502, 11.49999999999999645 ) ) ;
#44649=LINE ( 'NONE', #75578, #39173 ) ;
#44655=VERTEX_POINT ( 'NONE', #71370 ) ;
#44656=CARTESIAN_POINT ( 'NONE',  ( -102.6235477340627256, -24.66019654487200086, 8.947790411086115725 ) ) ;
#44659=CARTESIAN_POINT ( 'NONE',  ( -110.5228709571500758, -23.47593901973090524, -1.443836447538996204 ) ) ;
#44660=AXIS2_PLACEMENT_3D ( 'NONE', #40744, #64108, #10293 ) ;
#44661=CARTESIAN_POINT ( 'NONE',  ( -31.52287095715008292, -24.33927499327854349, 9.819080762295818943 ) ) ;
#44662=CARTESIAN_POINT ( 'NONE',  ( 3.315226082619958881, 19.80964767386612380, -1.500000000000002220 ) ) ;
#44667=CARTESIAN_POINT ( 'NONE',  ( -117.6228709571500275, -24.33927499327853994, 9.819080762295810061 ) ) ;
#44668=VECTOR ( 'NONE', #82246, 1000.000000000000114 ) ;
#44669=EDGE_CURVE ( 'NONE', #4924, #66877, #47531, .T. ) ;
#44670=B_SPLINE_CURVE_WITH_KNOTS ( 'NONE', 3,
 ( #59485, #90427, #20902, #82805, #33401, #9568, #56270, #64393, #85696, #16177, #63887, #94297, #40534, #1470, #71484, #78561 ),
 .UNSPECIFIED., .F., .F.,
 ( 4, 2, 2, 2, 2, 2, 2, 4 ),
 ( 6.992893892674702526E-18, 0.0002048719647680148778, 0.0004097439295360227624, 0.0008194878590720570174, 0.001024359823840074795, 0.001229231788608092357, 0.001434103753376110351, 0.001638975718144127913 ),
 .UNSPECIFIED. ) ;
#44672=CARTESIAN_POINT ( 'NONE',  ( 9.452765381649220089, 20.79790602042944414, 11.49999999999999645 ) ) ;
#44673=CARTESIAN_POINT ( 'NONE',  ( -102.5228709571500758, -24.33832256527048088, 0.1851278514138648412 ) ) ;
#44674=CARTESIAN_POINT ( 'NONE',  ( -82.62287095715005592, -24.65952944569304606, 1.056160979905699016 ) ) ;
#44676=DIRECTION ( 'NONE',  ( -3.773278334453079030E-23, 0.9999999999976377785, 2.173523156925979128E-06 ) ) ;
#44677=CARTESIAN_POINT ( 'NONE',  ( -117.5562042904833930, -23.47596703998600631, 11.44779298504227683 ) ) ;
#44678=CARTESIAN_POINT ( 'NONE',  ( -73.52287095715007581, -23.47593901973090169, -1.443836447538996870 ) ) ;
#44680=CARTESIAN_POINT ( 'NONE',  ( -17.59887021274124663, -10.25344800880639262, -1.500000000000002220 ) ) ;
#44681=B_SPLINE_CURVE_WITH_KNOTS ( 'NONE', 3,
 ( #24698, #9484, #24205, #86607 ),
 .UNSPECIFIED., .F., .F.,
 ( 4, 4 ),
 ( 1.387778780781445676E-17, 0.0001000000000000028508 ),
 .UNSPECIFIED. ) ;
#44682=ORIENTED_EDGE ( 'NONE', *, *, #39586, .T. ) ;
#44683=B_SPLINE_CURVE_WITH_KNOTS ( 'NONE', 3,
 ( #96496, #88899, #97496, #28477 ),
 .UNSPECIFIED., .F., .F.,
 ( 4, 4 ),
 ( 0.4691036948738852019, 0.4701044419146508946 ),
 .UNSPECIFIED. ) ;
#44684=CARTESIAN_POINT ( 'NONE',  ( 15.56936346670522120, 16.85858822313069894, -1.500000000000002220 ) ) ;
#44687=CARTESIAN_POINT ( 'NONE',  ( -108.5519249696069579, -24.35071581493544457, 9.817618358456016381 ) ) ;
#44688=CARTESIAN_POINT ( 'NONE',  ( -77.64260741054584969, -23.73791477778911840, 11.05961554403170588 ) ) ;
#44689=CARTESIAN_POINT ( 'NONE',  ( -40.62287095715007013, -24.62226745350437440, 0.9660975649728171799 ) ) ;
#44690=CARTESIAN_POINT ( 'NONE',  ( 17.81766572339076404, -11.58780717566545526, 11.49999999999999645 ) ) ;
#44692=AXIS2_PLACEMENT_3D ( 'NONE', #9211, #55915, #71630 ) ;
#44694=CARTESIAN_POINT ( 'NONE',  ( -15.96568504569681402, -15.38390974582250692, 11.49999999999998934 ) ) ;
#44695=CARTESIAN_POINT ( 'NONE',  ( 6.296002175621457475, 19.65409743616946514, 11.49999999999998934 ) ) ;
#44696=VERTEX_POINT ( 'NONE', #17064 ) ;
#44697=ORIENTED_EDGE ( 'NONE', *, *, #34197, .F. ) ;
#44699=CARTESIAN_POINT ( 'NONE',  ( -121.6228709571500701, -23.73907113216991860, -1.053371485793222595 ) ) ;
#44700=ORIENTED_EDGE ( 'NONE', *, *, #52589, .T. ) ;
#44702=CARTESIAN_POINT ( 'NONE',  ( -124.4728709570019873, -25.30556170156495455, 4.804051544042280852 ) ) ;
#44703=CARTESIAN_POINT ( 'NONE',  ( -111.5203643720066680, -23.73791477778912551, 11.05961554403170055 ) ) ;
#44705=CARTESIAN_POINT ( 'NONE',  ( 2.677173591928626806, -20.63698567995287902, -1.500000000000002220 ) ) ;
#44706=CARTESIAN_POINT ( 'NONE',  ( -0.2038501785326352067, 21.78777694363981254, 11.49999999999999645 ) ) ;
#44707=CARTESIAN_POINT ( 'NONE',  ( -51.32890343732908889, -25.08217282722072738, 7.322960462340015297 ) ) ;
#44708=CARTESIAN_POINT ( 'NONE',  ( -77.62287095715007013, -23.48786465467241413, 11.44779295918254469 ) ) ;
#44709=CARTESIAN_POINT ( 'NONE',  ( -115.5877649471882904, -24.83618233451451118, 1.606449574219534826 ) ) ;
#44710=CARTESIAN_POINT ( 'NONE',  ( -17.93832129671990572, 13.47109510200611560, 11.49999999999998934 ) ) ;
#44715=VERTEX_POINT ( 'NONE', #16057 ) ;
#44716=VERTEX_POINT ( 'NONE', #55650 ) ;
#44717=CARTESIAN_POINT ( 'NONE',  ( -99.83817514626852585, -25.31070701350142116, 5.349196373867116883 ) ) ;
#44719=AXIS2_PLACEMENT_3D ( 'NONE', #97212, #83978, #37808 ) ;
#44721=CARTESIAN_POINT ( 'NONE',  ( -15.80959461918071618, 14.24510877297761446, -1.500000000000002220 ) ) ;
#44722=ORIENTED_EDGE ( 'NONE', *, *, #76328, .T. ) ;
#44725=CARTESIAN_POINT ( 'NONE',  ( 15.37114825158464271, 14.37155165002682544, 11.49999999999998934 ) ) ;
#44726=CARTESIAN_POINT ( 'NONE',  ( -55.52287095715006870, -23.47596703998600631, 11.44779298504228926 ) ) ;
#44729=CARTESIAN_POINT ( 'NONE',  ( -65.52287095715006160, -24.91570333825770334, 8.075032458260364976 ) ) ;
#44730=CARTESIAN_POINT ( 'NONE',  ( 17.58553779993395594, 13.13030503331179411, -1.500000000000002220 ) ) ;
#44733=CARTESIAN_POINT ( 'NONE',  ( -40.09699101898657148, -25.29459747820068571, 5.519299892252927719 ) ) ;
#44736=EDGE_CURVE ( 'NONE', #63555, #32994, #87079, .T. ) ;
#44738=EDGE_CURVE ( 'NONE', #7487, #76771, #5232, .T. ) ;
#44739=CARTESIAN_POINT ( 'NONE',  ( -84.51016183175109120, -24.15620529776628445, 10.23563542870660292 ) ) ;
#44741=EDGE_CURVE ( 'NONE', #31278, #33587, #93184, .T. ) ;
#44743=CARTESIAN_POINT ( 'NONE',  ( 1.764508054474889009, 21.21474994468914943, -1.500000000000002220 ) ) ;
#44744=LINE ( 'NONE', #29003, #95281 ) ;
#44745=CARTESIAN_POINT ( 'NONE',  ( -107.5924962624403207, -23.96169478059713853, 10.65365249895717348 ) ) ;
#44746=CARTESIAN_POINT ( 'NONE',  ( -89.52287095715009002, -24.66019654487200441, 8.947790411086119278 ) ) ;
#44747=CARTESIAN_POINT ( 'NONE',  ( -70.52287095715011844, -24.82558206586151073, 1.605769216559629342 ) ) ;
#44748=CARTESIAN_POINT ( 'NONE',  ( -20.52357230491503159, 9.176553703681571861, -1.500000000000002220 ) ) ;
#44751=CARTESIAN_POINT ( 'NONE',  ( -98.94665561451864733, -25.22304042422490511, 6.503500078851421229 ) ) ;
#44752=CARTESIAN_POINT ( 'NONE',  ( -18.14765110722914798, -7.448729197826248871, 11.49999999999999645 ) ) ;
#44753=CARTESIAN_POINT ( 'NONE',  ( -99.13316617824068544, -25.28856576242281662, 4.187040092130447810 ) ) ;
#44754=CARTESIAN_POINT ( 'NONE',  ( -82.52287095715004739, -23.73907113217677889, -1.053371485781116723 ) ) ;
#44755=EDGE_CURVE ( 'NONE', #30329, #69394, #95996, .T. ) ;
#44757=CARTESIAN_POINT ( 'NONE',  ( -88.62862753172657904, -24.35071581493543746, 9.817618358456025263 ) ) ;
#44761=CARTESIAN_POINT ( 'NONE',  ( -51.52287095715005449, -24.66019654487199375, 8.947790411086119278 ) ) ;
#44762=CARTESIAN_POINT ( 'NONE',  ( 3.669390655483735220, -19.36157329643844704, 11.49999999999998934 ) ) ;
#44763=EDGE_CURVE ( 'NONE', #90373, #46797, #82695, .T. ) ;
#44764=ORIENTED_EDGE ( 'NONE', *, *, #68587, .T. ) ;
#44765=B_SPLINE_CURVE_WITH_KNOTS ( 'NONE', 3,
 ( #6353, #45921, #30681, #53539 ),
 .UNSPECIFIED., .F., .F.,
 ( 4, 4 ),
 ( 0.000000000000000000, 1.000000000000000000 ),
 .UNSPECIFIED. ) ;
#44766=CARTESIAN_POINT ( 'NONE',  ( -108.5562042904833930, -23.47596703998600631, 11.44779298504227683 ) ) ;
#44770=ORIENTED_EDGE ( 'NONE', *, *, #44290, .T. ) ;
#44773=CARTESIAN_POINT ( 'NONE',  ( -107.6228709571500701, -24.66019654487199730, 8.947790411086124607 ) ) ;
#44775=CARTESIAN_POINT ( 'NONE',  ( -119.6228709571500559, -29.50248528299804818, 1.056150453629045360 ) ) ;
#44776=CARTESIAN_POINT ( 'NONE',  ( -99.62287095715016960, -23.96177878511308634, 10.65340807706329684 ) ) ;
#44777=CARTESIAN_POINT ( 'NONE',  ( -127.5228709571500616, -24.64898659630368627, 1.056161002820834804 ) ) ;
#44778=CARTESIAN_POINT ( 'NONE',  ( 4.555139465550277933, 19.45931829295258453, -1.500000000000002220 ) ) ;
#44780=CARTESIAN_POINT ( 'NONE',  ( -127.6228709571500559, -24.64898659630368627, 1.056161002820834804 ) ) ;
#44781=CARTESIAN_POINT ( 'NONE',  ( -45.58194095766508980, -24.73531770709095312, 8.716586749053515604 ) ) ;
#44786=CARTESIAN_POINT ( 'NONE',  ( -119.5185327869307059, -24.34968618360934656, 0.1864209137778924941 ) ) ;
#44789=CARTESIAN_POINT ( 'NONE',  ( -39.54608221933844447, -24.15543982623906416, -0.2315651400026678131 ) ) ;
#44794=FACE_OUTER_BOUND ( 'NONE', #99858, .T. ) ;
#44795=DIRECTION ( 'NONE',  ( -3.773278334453079618E-23, 0.9999999999976377785, 2.173523156925979975E-06 ) ) ;
#44796=VECTOR ( 'NONE', #92585, 1000.000000000000114 ) ;
#44797=ORIENTED_EDGE ( 'NONE', *, *, #96784, .F. ) ;
#44799=CARTESIAN_POINT ( 'NONE',  ( -20.21730713243277933, 1.494317884549376974, 11.49999999999998934 ) ) ;
#44800=DIRECTION ( 'NONE',  ( -3.773278334453079618E-23, 0.9999999999976377785, 2.173523156925979975E-06 ) ) ;
#44801=CARTESIAN_POINT ( 'NONE',  ( -53.62287095715004881, -23.48783264082478084, -1.443836473390070596 ) ) ;
#44802=AXIS2_PLACEMENT_3D ( 'NONE', #81597, #12068, #19185 ) ;
#44803=CARTESIAN_POINT ( 'NONE',  ( -118.6228709571500559, -29.50250243563736774, 8.947779886222134493 ) ) ;
#44804=VERTEX_POINT ( 'NONE', #35798 ) ;
#44806=DIRECTION ( 'NONE',  ( 3.773278334444166432E-23, -1.000000000000000000, 0.000000000000000000 ) ) ;
#44807=CARTESIAN_POINT ( 'NONE',  ( -4.889416449700032530, -19.50743224814450016, -1.500000000000002220 ) ) ;
#44808=CARTESIAN_POINT ( 'NONE',  ( -20.60145385712877797, -4.430719527714695793, 11.49999999999999645 ) ) ;
#44810=CARTESIAN_POINT ( 'NONE',  ( -70.62753707971197059, -24.83644354573578994, 8.397322867130100121 ) ) ;
#44811=CARTESIAN_POINT ( 'NONE',  ( -16.84257673422482426, -14.26466048179180568, -1.500000000000002220 ) ) ;
#44812=B_SPLINE_CURVE_WITH_KNOTS ( 'NONE', 3,
 ( #43662, #5589, #51775, #58888, #89830, #27440 ),
 .UNSPECIFIED., .F., .F.,
 ( 4, 2, 4 ),
 ( 6.391158118963033910E-06, 0.001387004593080786580, 0.002767618028042609802 ),
 .UNSPECIFIED. ) ;
#44813=CARTESIAN_POINT ( 'NONE',  ( 11.66944253441096002, 16.90307425063352298, 11.49999999999998934 ) ) ;
#44814=CARTESIAN_POINT ( 'NONE',  ( -35.62287095715005592, -24.99132157543083821, 2.256160258750667502 ) ) ;
#44815=CARTESIAN_POINT ( 'NONE',  ( -35.62287095715005592, -29.50248528299804818, 1.056150453629031594 ) ) ;
#44816=ORIENTED_EDGE ( 'NONE', *, *, #99542, .T. ) ;
#44818=ORIENTED_EDGE ( 'NONE', *, *, #35629, .F. ) ;
#44819=CARTESIAN_POINT ( 'NONE',  ( -99.30746832622341458, -25.20873971062084706, 3.386897128527919243 ) ) ;
#44820=CARTESIAN_POINT ( 'NONE',  ( -129.9395376238167046, -23.47596703998600631, 11.44779298504227860 ) ) ;
#44822=EDGE_LOOP ( 'NONE', ( #12691, #70141, #78600, #76993, #48941 ) ) ;
#44823=CARTESIAN_POINT ( 'NONE',  ( -65.62287095715005592, -23.48783264082478084, -1.443836473390067265 ) ) ;
#44824=CARTESIAN_POINT ( 'NONE',  ( -31.62287095715005236, -23.47593901973091235, -1.443836447539013301 ) ) ;
#44826=CARTESIAN_POINT ( 'NONE',  ( -7.762539992054180438, 19.06225842855939234, -1.500000000000002220 ) ) ;
#44827=CARTESIAN_POINT ( 'NONE',  ( 18.49883484089910723, -11.16122333755292750, 11.49999999999999645 ) ) ;
#44828=VERTEX_POINT ( 'NONE', #81971 ) ;
#44829=CARTESIAN_POINT ( 'NONE',  ( -99.17846093192173385, -25.28926427284505607, 4.366343918064007568 ) ) ;
#44830=VECTOR ( 'NONE', #86501, 1000.000000000000114 ) ;
#44832=CARTESIAN_POINT ( 'NONE',  ( 10.24050353823403192, -19.87907451059620456, -1.500000000000002220 ) ) ;
#44833=CARTESIAN_POINT ( 'NONE',  ( -34.52287095715006160, -23.48786465467240347, 11.44779295918255357 ) ) ;
#44834=CARTESIAN_POINT ( 'NONE',  ( -52.62287095715005592, -29.50250243563736774, 8.947779886222146928 ) ) ;
#44837=CARTESIAN_POINT ( 'NONE',  ( -49.64567687034262633, -23.96169478059712432, 10.65365249895718414 ) ) ;
#44839=CARTESIAN_POINT ( 'NONE',  ( 20.36350155627077640, -4.707376482769925374, 11.49999999999998934 ) ) ;
#44841=CARTESIAN_POINT ( 'NONE',  ( -67.50569153577386317, -24.15620529776628800, 10.23563542870660115 ) ) ;
#44842=ORIENTED_EDGE ( 'NONE', *, *, #35016, .F. ) ;
#44844=CARTESIAN_POINT ( 'NONE',  ( -100.5497400620557187, -24.52399227489127398, 9.353111116836526406 ) ) ;
#44845=CARTESIAN_POINT ( 'NONE',  ( 20.77832821955112408, -3.674247523096572099, -1.500000000000002220 ) ) ;
#44847=CARTESIAN_POINT ( 'NONE',  ( -117.5555609497473597, -23.96119346886881019, -0.6495511937831994764 ) ) ;
#44848=DIRECTION ( 'NONE',  ( 0.000000000000000000, 0.9999999999976377785, 2.173523156925979128E-06 ) ) ;
#44849=ADVANCED_FACE ( 'NONE', ( #96689 ), #89086, .F. ) ;
#44850=CARTESIAN_POINT ( 'NONE',  ( 9.495391690522565042, 19.61495305411445500, 11.49999999999998934 ) ) ;
#44853=CARTESIAN_POINT ( 'NONE',  ( -81.62287095715005592, -24.64898659630528854, 1.056161002820826145 ) ) ;
#44855=CARTESIAN_POINT ( 'NONE',  ( 11.36066313177254905, -18.55813952095733654, -1.500000000000002220 ) ) ;
#44856=CARTESIAN_POINT ( 'NONE',  ( -71.39239612577370053, -25.24674124963215505, 5.186401910093661805 ) ) ;
#44857=CARTESIAN_POINT ( 'NONE',  ( 3.003370282714790562, 22.13870467353671856, 11.49999999999999645 ) ) ;
#44859=CARTESIAN_POINT ( 'NONE',  ( -45.62287095715004170, -24.92579138211019085, 1.929029949965659130 ) ) ;
#44860=CARTESIAN_POINT ( 'NONE',  ( -117.5228709571500758, -23.72747288104470087, -1.053458166803225682 ) ) ;
#44862=ORIENTED_EDGE ( 'NONE', *, *, #37769, .F. ) ;
#44864=EDGE_CURVE ( 'NONE', #53293, #75504, #26987, .T. ) ;
#44869=CARTESIAN_POINT ( 'NONE',  ( -10.94853654022341516, 18.13385389444049522, -1.500000000000002220 ) ) ;
#44872=CARTESIAN_POINT ( 'NONE',  ( -64.62287095715005592, -29.50247984919015209, -1.443849546365056913 ) ) ;
#44875=CARTESIAN_POINT ( 'NONE',  ( -9.899997732206244905, -16.63842163800745766, 11.49999999999998934 ) ) ;
#44876=EDGE_CURVE ( 'NONE', #63805, #60463, #28252, .T. ) ;
#44877=CARTESIAN_POINT ( 'NONE',  ( -38.52287095715006870, -24.64898659630367206, 1.056161002820819261 ) ) ;
#44880=CARTESIAN_POINT ( 'NONE',  ( 6.036767712469883307, 18.47306877840545170, 11.49999999999999645 ) ) ;
#44881=LINE ( 'NONE', #51987, #47105 ) ;
#44883=ORIENTED_EDGE ( 'NONE', *, *, #11460, .T. ) ;
#44885=PLANE ( 'NONE',  #91185 ) ;
#44889=CARTESIAN_POINT ( 'NONE',  ( -19.37001648656083574, -3.113731218521536004, 11.49999999999998934 ) ) ;
#44890=CARTESIAN_POINT ( 'NONE',  ( -46.58714575211884323, -24.34968618360932879, 0.1864209137778778391 ) ) ;
#44891=ORIENTED_EDGE ( 'NONE', *, *, #66071, .F. ) ;
#44892=CARTESIAN_POINT ( 'NONE',  ( 16.61904782137575154, -13.72857183568914685, -1.500000000000002220 ) ) ;
#44895=CARTESIAN_POINT ( 'NONE',  ( -119.6228709571500559, -29.50250786944525672, 11.44777988621622811 ) ) ;
#44896=DIRECTION ( 'NONE',  ( 3.773278334444166432E-23, -1.000000000000000000, 0.000000000000000000 ) ) ;
#44897=CARTESIAN_POINT ( 'NONE',  ( -99.92039718326317654, -25.27473246999687007, 3.410800712176911720 ) ) ;
#44898=CARTESIAN_POINT ( 'NONE',  ( 22.88022663504679599, 2.825535151426334934, -1.500000000000002220 ) ) ;
#44901=CARTESIAN_POINT ( 'NONE',  ( -129.6228709571500133, -23.48783264082478794, -1.443836473390056607 ) ) ;
#44902=CARTESIAN_POINT ( 'NONE',  ( -13.64458216870221818, 14.86554040878868044, 11.49999999999999645 ) ) ;
#44903=CARTESIAN_POINT ( 'NONE',  ( -84.62287095715005592, -23.72773821059536559, 11.05748984161097503 ) ) ;
#44904=PLANE ( 'NONE',  #27433 ) ;
#44905=CARTESIAN_POINT ( 'NONE',  ( -89.62287095715004170, -29.50250786944525672, 11.44777988621623344 ) ) ;
#44907=CARTESIAN_POINT ( 'NONE',  ( -30.64751926837171325, -23.47596703998600631, 11.44779298504228038 ) ) ;
#44908=CARTESIAN_POINT ( 'NONE',  ( 7.211006999188390942, 18.53272205163514030, -1.500000000000002220 ) ) ;
#44909=CARTESIAN_POINT ( 'NONE',  ( -113.5517726272361045, -24.51314013834315375, 0.6176544820404169522 ) ) ;
#44910=CARTESIAN_POINT ( 'NONE',  ( -8.281543130087330340, -17.94227898472161797, -1.500000000000002220 ) ) ;
#44914=CARTESIAN_POINT ( 'NONE',  ( -125.6228709571500275, -24.14406661707773338, 10.28769366152062226 ) ) ;
#44916=CARTESIAN_POINT ( 'NONE',  ( -17.42616458466809704, -11.11377323884725321, 11.49999999999999645 ) ) ;
#44918=DIRECTION ( 'NONE',  ( -3.773278334453079030E-23, 0.9999999999976377785, 2.173523156925979128E-06 ) ) ;
#44920=DIRECTION ( 'NONE',  ( -3.773278334444166432E-23, 1.000000000000000000, 0.000000000000000000 ) ) ;
#44921=CARTESIAN_POINT ( 'NONE',  ( -35.55620429048339304, -23.47596703998600276, 11.44779298504227505 ) ) ;
#44922=CARTESIAN_POINT ( 'NONE',  ( 22.16846167567618053, -4.910139430472912458, 11.49999999999999645 ) ) ;
#44923=ORIENTED_EDGE ( 'NONE', *, *, #17458, .T. ) ;
#44924=B_SPLINE_SURFACE_WITH_KNOTS ( 'NONE', 3, 3, ( 
 ( #30455, #60424, #7618, #14718 ),
 ( #38568, #68030, #84232, #69525 ),
 ( #91848, #6114, #91349, #84736 ),
 ( #46183, #21824, #45685, #76608 ),
 ( #52800, #15225, #69017, #54309 ),
 ( #7, #30950, #83734, #61916 ),
 ( #99942, #61419, #77613, #92843 ) ),
 .UNSPECIFIED., .F., .F., .F.,
 ( 4, 3, 4 ),
 ( 4, 4 ),
 ( 0.7945040050992243641, 0.8970133687736503436, 0.9995227324480764342 ),
 ( 0.7896946696024070844, 0.7910719696203489804 ),
 .UNSPECIFIED. ) ;
#44925=FACE_OUTER_BOUND ( 'NONE', #61214, .T. ) ;
#44927=CARTESIAN_POINT ( 'NONE',  ( 0.4983251850863967269, 20.17815531296474418, 11.49999999999998934 ) ) ;
#44928=CARTESIAN_POINT ( 'NONE',  ( -63.62365437609576446, -24.65952944569304250, 1.056160979905695463 ) ) ;
#44929=DIRECTION ( 'NONE',  ( -3.773278334453079618E-23, 0.9999999999976377785, 2.173523156925979975E-06 ) ) ;
#44930=ORIENTED_EDGE ( 'NONE', *, *, #91785, .F. ) ;
#44931=VECTOR ( 'NONE', #79557, 1000.000000000000114 ) ;
#44933=CARTESIAN_POINT ( 'NONE',  ( -101.3738023147422780, -29.50249165161862663, 3.986241424695394109 ) ) ;
#44934=CARTESIAN_POINT ( 'NONE',  ( 21.91704834537361180, 6.644925864936762849, 11.49999999999998934 ) ) ;
#44936=CARTESIAN_POINT ( 'NONE',  ( 0.9236959384754221958, 21.56878955078795812, -1.500000000000002220 ) ) ;
#44937=CARTESIAN_POINT ( 'NONE',  ( -123.5918554517772918, -23.48783264082477373, -1.443836473390086361 ) ) ;
#44938=CARTESIAN_POINT ( 'NONE',  ( -34.52200860028750640, -23.48783264082478084, -1.443836473390076591 ) ) ;
#44939=CARTESIAN_POINT ( 'NONE',  ( 20.83135763335140922, 1.668377004047274959, 11.49999999999999645 ) ) ;
#44942=CARTESIAN_POINT ( 'NONE',  ( 9.413913215453616701, -19.89622248225912315, -1.500000000000002220 ) ) ;
#44944=CARTESIAN_POINT ( 'NONE',  ( -105.5855865933814215, -24.92592662359561473, 8.075495903017998245 ) ) ;
#44945=CARTESIAN_POINT ( 'NONE',  ( -41.68940843163829868, -25.29087182211354090, 3.512445110864212516 ) ) ;
#44946=ORIENTED_EDGE ( 'NONE', *, *, #49409, .F. ) ;
#44948=CARTESIAN_POINT ( 'NONE',  ( -90.58933947920019136, -24.52399227489127398, 9.353111116836531735 ) ) ;
#44949=VERTEX_POINT ( 'NONE', #83452 ) ;
#44950=CARTESIAN_POINT ( 'NONE',  ( -93.52287095715006160, -23.47596703998600631, 11.44779298504228393 ) ) ;
#44956=CARTESIAN_POINT ( 'NONE',  ( -57.63244684718339528, -24.34968618360933590, 0.1864209137778796155 ) ) ;
#44957=CARTESIAN_POINT ( 'NONE',  ( -18.16121111207539940, 9.348575961806686152, -1.500000000000002220 ) ) ;
#44960=CARTESIAN_POINT ( 'NONE',  ( -115.6228709571500701, -24.14406661707771207, 10.28769366152061160 ) ) ;
#44961=B_SPLINE_CURVE_WITH_KNOTS ( 'NONE', 3,
 ( #98105, #18994, #34729, #3303, #35732, #81404, #74771, #73297, #36226, #49973, #66704, #11387, #11883, #82391, #34235, #42365 ),
 .UNSPECIFIED., .F., .F.,
 ( 4, 2, 2, 2, 2, 2, 2, 4 ),
 ( 0.000000000000000000, 0.0002722372812524201055, 0.0005444745625048402109, 0.001088949125009681506, 0.001361186406262094185, 0.001633423687514507297, 0.001905660968766919976, 0.002177898250019332654 ),
 .UNSPECIFIED. ) ;
#44963=CARTESIAN_POINT ( 'NONE',  ( -25.63531995026274402, -24.86348392168161681, 6.224458436948604678 ) ) ;
#44964=ORIENTED_EDGE ( 'NONE', *, *, #39985, .T. ) ;
#44966=CARTESIAN_POINT ( 'NONE',  ( -29.21927636257191807, -25.26247907303463336, 7.471890645913414453 ) ) ;
#44967=CARTESIAN_POINT ( 'NONE',  ( 2.040502595053849788, 20.68626321094233944, -1.500000000000002220 ) ) ;
#44968=VERTEX_POINT ( 'NONE', #45908 ) ;
#44970=ORIENTED_EDGE ( 'NONE', *, *, #22030, .F. ) ;
#44973=ORIENTED_EDGE ( 'NONE', *, *, #60446, .T. ) ;
#44976=EDGE_CURVE ( 'NONE', #41736, #47247, #61141, .T. ) ;
#44978=CARTESIAN_POINT ( 'NONE',  ( -105.6228709571500559, -23.47593901973091235, -1.443836447538999312 ) ) ;
#44979=CARTESIAN_POINT ( 'NONE',  ( -92.58855183542770817, -24.35071581493543391, 9.817618358456025263 ) ) ;
#44980=CARTESIAN_POINT ( 'NONE',  ( -95.55620429048339304, -23.47596703998600631, 11.44779298504227683 ) ) ;
#44981=CARTESIAN_POINT ( 'NONE',  ( -21.88945651911318535, 3.243594245096953710, 11.49999999999999645 ) ) ;
#44982=ORIENTED_EDGE ( 'NONE', *, *, #86723, .T. ) ;
#44983=CARTESIAN_POINT ( 'NONE',  ( -108.5535964976718333, -24.15543982623908192, -0.2315651400026445539 ) ) ;
#44985=CARTESIAN_POINT ( 'NONE',  ( -21.16596634977960179, 8.012090315382277339, 11.49999999999998934 ) ) ;
#44988=CARTESIAN_POINT ( 'NONE',  ( -115.6302133932577334, -23.85049219812686871, 10.88485053497526778 ) ) ;
#44989=ORIENTED_EDGE ( 'NONE', *, *, #11216, .F. ) ;
#44990=EDGE_CURVE ( 'NONE', #77156, #18231, #90573, .T. ) ;
#44991=EDGE_LOOP ( 'NONE', ( #12099, #59719, #99839, #36940 ) ) ;
#44992=AXIS2_PLACEMENT_3D ( 'NONE', #28650, #66740, #21023 ) ;
#44995=CARTESIAN_POINT ( 'NONE',  ( -11.83016301840747175, -16.26703346747452983, -1.500000000000002220 ) ) ;
#44998=B_SPLINE_CURVE_WITH_KNOTS ( 'NONE', 3,
 ( #30164, #94061, #14437, #45409 ),
 .UNSPECIFIED., .F., .F.,
 ( 4, 4 ),
 ( 0.9294473336260299368, 0.9304480806667954074 ),
 .UNSPECIFIED. ) ;
#45000=CARTESIAN_POINT ( 'NONE',  ( -21.40455707349245529, -6.346402434563959361, -1.500000000000002220 ) ) ;
#45001=ADVANCED_FACE ( 'NONE', ( #6828 ), #22045, .F. ) ;
#45007=CARTESIAN_POINT ( 'NONE',  ( -63.52287095715009002, -23.73907113216989728, -1.053371485793251239 ) ) ;
#45010=CARTESIAN_POINT ( 'NONE',  ( 8.254404603115069960, -17.72612730319335839, -1.500000000000002220 ) ) ;
#45011=CARTESIAN_POINT ( 'NONE',  ( -47.52287095715006160, -23.48783264083458988, -1.443836473374825236 ) ) ;
#45012=CARTESIAN_POINT ( 'NONE',  ( 14.45597713831175035, -15.85640774750547344, 11.49999999999998934 ) ) ;
#45013=CARTESIAN_POINT ( 'NONE',  ( -25.60037597819128763, -24.92775154704442286, 3.875572922187972225 ) ) ;
#45014=PLANE ( 'NONE',  #27625 ) ;
#45016=CARTESIAN_POINT ( 'NONE',  ( 13.72848742581335912, -18.28091200367991576, -1.500000000000002220 ) ) ;
#45019=CARTESIAN_POINT ( 'NONE',  ( -106.6344572697143462, -23.48786465467241769, 11.44779295918253581 ) ) ;
#45020=CARTESIAN_POINT ( 'NONE',  ( -125.5895376238167245, -23.48783264082479505, -1.443836473390057273 ) ) ;
#45021=CARTESIAN_POINT ( 'NONE',  ( -19.24466553037914807, -5.328869878250761971, 11.49999999999999645 ) ) ;
#45022=CARTESIAN_POINT ( 'NONE',  ( -111.5562042904833930, -23.47593901973091235, -1.443836447538999312 ) ) ;
#45024=CARTESIAN_POINT ( 'NONE',  ( -74.63034837134625832, -24.35071581493544102, 9.817618358456019934 ) ) ;
#45027=DIRECTION ( 'NONE',  ( 0.000000000000000000, -0.9999999999976377785, -2.173523156925979128E-06 ) ) ;
#45030=CARTESIAN_POINT ( 'NONE',  ( -16.45766974254678061, 14.19212061201335473, -1.500000000000002220 ) ) ;
#45031=CARTESIAN_POINT ( 'NONE',  ( -77.55620429048339304, -24.66019654487199730, 8.947790411086124607 ) ) ;
#45032=CARTESIAN_POINT ( 'NONE',  ( -10.75157073690095721, 16.42123490324765811, -1.500000000000002220 ) ) ;
#45033=LINE ( 'NONE', #6951, #63707 ) ;
#45034=EDGE_CURVE ( 'NONE', #85354, #1776, #18537, .T. ) ;
#45039=CARTESIAN_POINT ( 'NONE',  ( -14.05295919346176170, -14.94737400546395456, 11.49999999999999645 ) ) ;
#45041=CARTESIAN_POINT ( 'NONE',  ( -93.52287095715009002, -23.48783264082477018, -1.443836473390088360 ) ) ;
#45043=EDGE_CURVE ( 'NONE', #9013, #20503, #36682, .T. ) ;
#45046=CARTESIAN_POINT ( 'NONE',  ( -78.62287095715005592, -24.64898659630367916, 1.056161002820826145 ) ) ;
#45048=PLANE ( 'NONE',  #61392 ) ;
#45050=AXIS2_PLACEMENT_3D ( 'NONE', #100232, #85528, #799 ) ;
#45051=CARTESIAN_POINT ( 'NONE',  ( -3.594920434497504758, 22.80983129501555950, 11.49999999999999645 ) ) ;
#45052=CARTESIAN_POINT ( 'NONE',  ( -19.53289989604362376, -11.71160353944097920, -1.500000000000002220 ) ) ;
#45054=B_SPLINE_SURFACE_WITH_KNOTS ( 'NONE', 3, 3, ( 
 ( #3181, #26507, #4167, #50344 ),
 ( #87903, #57471, #73184, #17889 ),
 ( #25996, #81784, #18386, #65590 ),
 ( #49355, #19870, #19378, #50845 ),
 ( #34121, #3673, #97006, #12255 ),
 ( #49860, #89397, #74172, #66091 ),
 ( #80791, #35618, #72186, #96012 ) ),
 .UNSPECIFIED., .F., .F., .F.,
 ( 4, 3, 4 ),
 ( 4, 4 ),
 ( 0.0004766839783817761926, 0.1029713700210894839, 0.2054660560637971978 ),
 ( 0.4196007365068247785, 0.4208070640716953803 ),
 .UNSPECIFIED. ) ;
#45055=CARTESIAN_POINT ( 'NONE',  ( -88.52287095715006160, -24.65952944569304606, 1.056160979905700570 ) ) ;
#45057=CARTESIAN_POINT ( 'NONE',  ( -110.9909297185884327, -25.15277794460069671, 6.986250878905948980 ) ) ;
#45058=CARTESIAN_POINT ( 'NONE',  ( -69.52287095715006160, -24.64898659630367916, 1.056161002820824368 ) ) ;
#45059=CARTESIAN_POINT ( 'NONE',  ( -8.322136096487577461, -20.27582920440508829, 11.49999999999998934 ) ) ;
#45063=CARTESIAN_POINT ( 'NONE',  ( -31.62287095715005236, -29.50247984919015209, -1.443849546365062242 ) ) ;
#45064=CARTESIAN_POINT ( 'NONE',  ( -49.16098733389834763, -25.13996252305080503, 7.003495811256752468 ) ) ;
#45066=CARTESIAN_POINT ( 'NONE',  ( -73.55620429048340725, -23.48786465467241058, 11.44779295918255002 ) ) ;
#45067=ORIENTED_EDGE ( 'NONE', *, *, #78635, .T. ) ;
#45068=CARTESIAN_POINT ( 'NONE',  ( 14.97853827808193294, 13.91023239937271860, 11.49999999999998934 ) ) ;
#45071=ORIENTED_EDGE ( 'NONE', *, *, #17957, .F. ) ;
#45073=CARTESIAN_POINT ( 'NONE',  ( -17.35246277222573141, 15.15038115719275424, -1.500000000000002220 ) ) ;
#45074=CARTESIAN_POINT ( 'NONE',  ( -95.62287095715005592, -25.00158670708909625, 2.256160236439165967 ) ) ;
#45075=CARTESIAN_POINT ( 'NONE',  ( 8.147030896810244727, 18.52525024547675869, -1.500000000000002220 ) ) ;
#45076=ORIENTED_EDGE ( 'NONE', *, *, #86923, .F. ) ;
#45077=CARTESIAN_POINT ( 'NONE',  ( -28.20286574835018811, -25.11719900286342266, 4.027978703335532096 ) ) ;
#45079=CARTESIAN_POINT ( 'NONE',  ( -41.82896759111799412, -25.30795331362449829, 4.562858401357758886 ) ) ;
#45080=CARTESIAN_POINT ( 'NONE',  ( -89.81226385320381667, -25.32958633408183857, 5.296208831758598023 ) ) ;
#45081=FACE_OUTER_BOUND ( 'NONE', #74285, .T. ) ;
#45082=CARTESIAN_POINT ( 'NONE',  ( -13.99230614532761052, -16.21612836239924960, 11.49999999999999645 ) ) ;
#45083=VERTEX_POINT ( 'NONE', #33168 ) ;
#45085=CARTESIAN_POINT ( 'NONE',  ( -43.62287095715004881, -23.48783264082477729, -1.443836473390071928 ) ) ;
#45086=ORIENTED_EDGE ( 'NONE', *, *, #24231, .T. ) ;
#45087=CARTESIAN_POINT ( 'NONE',  ( 8.970943996638910178, -18.66293075132952950, -1.500000000000002220 ) ) ;
#45089=CARTESIAN_POINT ( 'NONE',  ( -80.58953762381671027, -23.48783264082478439, -1.443836473390065489 ) ) ;
#45090=VERTEX_POINT ( 'NONE', #70235 ) ;
#45091=CARTESIAN_POINT ( 'NONE',  ( -28.65223502837594793, -23.80851314359095738, -0.6495505116914124244 ) ) ;
#45094=AXIS2_PLACEMENT_3D ( 'NONE', #99775, #8954, #30283 ) ;
#45095=ORIENTED_EDGE ( 'NONE', *, *, #25712, .T. ) ;
#45096=B_SPLINE_CURVE_WITH_KNOTS ( 'NONE', 3,
 ( #78589, #3498, #16709, #55796 ),
 .UNSPECIFIED., .F., .F.,
 ( 4, 4 ),
 ( 0.000000000000000000, 9.999999999998897304E-05 ),
 .UNSPECIFIED. ) ;
#45097=CARTESIAN_POINT ( 'NONE',  ( -20.44905293368100985, -4.654758753755802836, -1.500000000000002220 ) ) ;
#45099=CARTESIAN_POINT ( 'NONE',  ( 3.092608977599853315, -21.74436839971096802, 11.49999999999999645 ) ) ;
#45100=DIRECTION ( 'NONE',  ( -3.773278334453080206E-23, 0.9999999999976377785, 2.173523156925979975E-06 ) ) ;
#45101=CARTESIAN_POINT ( 'NONE',  ( 19.01167203989450982, 12.12494712425435850, -1.500000000000002220 ) ) ;
#45102=CARTESIAN_POINT ( 'NONE',  ( -0.6469382494902750080, 20.97623560764392181, -1.500000000000002220 ) ) ;
#45108=EDGE_CURVE ( 'NONE', #94513, #18101, #55018, .T. ) ;
#45111=EDGE_CURVE ( 'NONE', #45090, #97756, #70738, .T. ) ;
#45112=FACE_OUTER_BOUND ( 'NONE', #99729, .T. ) ;
#45113=CARTESIAN_POINT ( 'NONE',  ( 21.49998558720804809, 0.1351929536555107336, -1.500000000000002220 ) ) ;
#45114=CARTESIAN_POINT ( 'NONE',  ( -105.5228709571500758, -24.82576562948885979, 8.398263436605498455 ) ) ;
#45115=VERTEX_POINT ( 'NONE', #48408 ) ;
#45116=CARTESIAN_POINT ( 'NONE',  ( -7.596101150008887082, -19.70107428960382734, -1.500000000000002220 ) ) ;
#45118=CARTESIAN_POINT ( 'NONE',  ( -42.62287095715004881, -29.50248528299804818, 1.056150453629031594 ) ) ;
#45119=CARTESIAN_POINT ( 'NONE',  ( -100.5228709571500758, -24.52232992886360918, 0.6492154411906000400 ) ) ;
#45121=CARTESIAN_POINT ( 'NONE',  ( -41.92287095715005307, -23.47593901973090169, -1.443836447538997980 ) ) ;
#45122=CARTESIAN_POINT ( 'NONE',  ( -15.96568504569681402, -15.38390974582250692, -1.500000000000002220 ) ) ;
#45123=CARTESIAN_POINT ( 'NONE',  ( -81.60466250293514179, -23.48786465467241413, 11.44779295918254824 ) ) ;
#45124=EDGE_CURVE ( 'NONE', #26773, #83907, #43879, .T. ) ;
#45127=CARTESIAN_POINT ( 'NONE',  ( -58.62287095715007013, -23.47596703998600276, 11.44779298504227683 ) ) ;
#45128=CARTESIAN_POINT ( 'NONE',  ( -77.52287095715006160, -24.65952944569304606, 1.056160979905698794 ) ) ;
#45129=CARTESIAN_POINT ( 'NONE',  ( -100.6334234393085154, -24.15503026093918137, -0.2815557561904373229 ) ) ;
#45130=CARTESIAN_POINT ( 'NONE',  ( -11.39837868854680814, -15.77482985264681403, 11.49999999999998934 ) ) ;
#45131=CARTESIAN_POINT ( 'NONE',  ( 20.27498964588844643, 6.839650151297337999, -1.500000000000002220 ) ) ;
#45135=CARTESIAN_POINT ( 'NONE',  ( -69.94583503291330828, -25.24888741496607381, 3.680065526283697874 ) ) ;
#45136=CARTESIAN_POINT ( 'NONE',  ( -3.801653518169780366, -22.29579330195574016, -1.500000000000002220 ) ) ;
#45138=ORIENTED_EDGE ( 'NONE', *, *, #57296, .F. ) ;
#45140=CARTESIAN_POINT ( 'NONE',  ( -97.55620429048337883, -24.64898659630528499, 1.056161002820831474 ) ) ;
#45141=CARTESIAN_POINT ( 'NONE',  ( 16.35176858736616978, 11.14859404531058473, 11.49999999999999645 ) ) ;
#45144=CARTESIAN_POINT ( 'NONE',  ( -37.52287095715006870, -24.66019654487199375, 8.947790411086122830 ) ) ;
#45145=CARTESIAN_POINT ( 'NONE',  ( -61.64687923781922763, -25.19045605819419364, 3.255062319851647956 ) ) ;
#45146=CARTESIAN_POINT ( 'NONE',  ( 16.85579979752674618, 13.57973486276658903, -1.500000000000002220 ) ) ;
#45147=CARTESIAN_POINT ( 'NONE',  ( -27.09174982187060365, -24.78434339138140885, 7.461775111898752755 ) ) ;
#45148=AXIS2_PLACEMENT_3D ( 'NONE', #44529, #52140, #44020 ) ;
#45149=CARTESIAN_POINT ( 'NONE',  ( 11.07193147992585835, -15.93265361536492364, -1.500000000000002220 ) ) ;
#45150=B_SPLINE_CURVE_WITH_KNOTS ( 'NONE', 3,
 ( #67055, #3651, #19358, #27976 ),
 .UNSPECIFIED., .F., .F.,
 ( 4, 4 ),
 ( 0.000000000000000000, 9.999999999994735322E-05 ),
 .UNSPECIFIED. ) ;
#45152=FACE_OUTER_BOUND ( 'NONE', #52828, .T. ) ;
#45153=CARTESIAN_POINT ( 'NONE',  ( 16.85830656838225039, -10.38424343889589707, 11.49999999999998934 ) ) ;
#45155=ORIENTED_EDGE ( 'NONE', *, *, #39782, .F. ) ;
#45156=B_SPLINE_CURVE_WITH_KNOTS ( 'NONE', 3,
 ( #99130, #99621, #22497, #62094 ),
 .UNSPECIFIED., .F., .F.,
 ( 4, 4 ),
 ( 0.000000000000000000, 9.999999999998897304E-05 ),
 .UNSPECIFIED. ) ;
#45157=CARTESIAN_POINT ( 'NONE',  ( 9.679018533540549640, -17.85022214266596308, 11.49999999999999645 ) ) ;
#45158=CARTESIAN_POINT ( 'NONE',  ( -111.5895376238167103, -24.66019654487199375, 8.947790411086121054 ) ) ;
#45162=CARTESIAN_POINT ( 'NONE',  ( -0.07511669896460689000, -22.07755530215571582, 0.1835287498755953650 ) ) ;
#45163=CARTESIAN_POINT ( 'NONE',  ( -95.52287095715006160, -24.99156044556203327, 7.747789690856173195 ) ) ;
#45164=CARTESIAN_POINT ( 'NONE',  ( -49.70686029532972583, -25.31601821332649038, 4.960083871316195214 ) ) ;
#45166=CARTESIAN_POINT ( 'NONE',  ( -95.62287095715008434, -24.52232992886363050, 0.6492154411906150280 ) ) ;
#45167=DIRECTION ( 'NONE',  ( -3.773278334453079030E-23, 0.9999999999976377785, 2.173523156925979128E-06 ) ) ;
#45168=CARTESIAN_POINT ( 'NONE',  ( -2.827821146493835425, 19.88259668395040691, 11.49999999999998934 ) ) ;
#45169=CARTESIAN_POINT ( 'NONE',  ( -79.62287095715005592, -23.47593901973091235, -1.443836447539004642 ) ) ;
#45171=CARTESIAN_POINT ( 'NONE',  ( -70.52287095715007581, -25.00158670708909625, 2.256160236439166411 ) ) ;
#45173=CARTESIAN_POINT ( 'NONE',  ( 15.01570752033863165, -17.30494853738164096, 11.49999999999999645 ) ) ;
#45174=CARTESIAN_POINT ( 'NONE',  ( -49.94769165354211538, -25.26258863353852746, 4.634773020030235280 ) ) ;
#45180=CARTESIAN_POINT ( 'NONE',  ( -41.86995616089613748, -25.27977532709532227, 4.210709737483026238 ) ) ;
#45182=CARTESIAN_POINT ( 'NONE',  ( 12.22771034161782566, -16.27230226814707947, -1.500000000000002220 ) ) ;
#45183=ORIENTED_EDGE ( 'NONE', *, *, #61961, .T. ) ;
#45184=CARTESIAN_POINT ( 'NONE',  ( 2.177599385301639323, -22.86303409451243596, 11.49999999999998934 ) ) ;
#45186=EDGE_CURVE ( 'NONE', #49833, #75137, #73007, .T. ) ;
#45190=FACE_OUTER_BOUND ( 'NONE', #69089, .T. ) ;
#45191=CARTESIAN_POINT ( 'NONE',  ( 7.950249384483326409, 19.69624408967213469, 11.49999999999999645 ) ) ;
#45192=ORIENTED_EDGE ( 'NONE', *, *, #31383, .F. ) ;
#45193=VERTEX_POINT ( 'NONE', #78330 ) ;
#45194=CARTESIAN_POINT ( 'NONE',  ( 18.11909884760711975, -12.84011383348296853, 11.49999999999998934 ) ) ;
#45195=CARTESIAN_POINT ( 'NONE',  ( -19.88974639711211623, -5.441847772814488948, 11.49999999999998934 ) ) ;
#45196=ORIENTED_EDGE ( 'NONE', *, *, #10854, .T. ) ;
#45197=EDGE_LOOP ( 'NONE', ( #27134, #71435, #29080, #88145 ) ) ;
#45198=PLANE ( 'NONE',  #18723 ) ;
#45200=VERTEX_POINT ( 'NONE', #1230 ) ;
#45202=VECTOR ( 'NONE', #18472, 1000.000000000000114 ) ;
#45205=LINE ( 'NONE', #60443, #97365 ) ;
#45206=CARTESIAN_POINT ( 'NONE',  ( 19.72710162658169608, 6.580912942549038469, -1.500000000000002220 ) ) ;
#45207=ADVANCED_FACE ( 'NONE', ( #77327 ), #32164, .F. ) ;
#45208=CARTESIAN_POINT ( 'NONE',  ( 1.801620404824296084, -21.73869551012647605, 11.49999999999999645 ) ) ;
#45209=CARTESIAN_POINT ( 'NONE',  ( -51.92861183494494526, -25.23934194637364214, 6.270802386038849541 ) ) ;
#45210=CARTESIAN_POINT ( 'NONE',  ( -98.94588073693361707, -25.21331259941279157, 6.500605466382517683 ) ) ;
#45211=CARTESIAN_POINT ( 'NONE',  ( 1.786768808452938950, -22.39398889530128756, 11.49999999999998934 ) ) ;
#45212=AXIS2_PLACEMENT_3D ( 'NONE', #78725, #58802, #19719 ) ;
#45213=CARTESIAN_POINT ( 'NONE',  ( -51.29599548036032530, -25.26334595364517455, 4.016965689284721641 ) ) ;
#45214=ORIENTED_EDGE ( 'NONE', *, *, #93238, .T. ) ;
#45215=CARTESIAN_POINT ( 'NONE',  ( -50.52287095715006160, -24.83620972994591725, 8.398175272781367440 ) ) ;
#45216=CARTESIAN_POINT ( 'NONE',  ( -69.52287095715006160, -24.64965694238407323, 8.947790433994200043 ) ) ;
#45219=ORIENTED_EDGE ( 'NONE', *, *, #83892, .F. ) ;
#45220=CARTESIAN_POINT ( 'NONE',  ( -57.52287095715005449, -29.50248528299804818, 1.056150453629034924 ) ) ;
#45222=EDGE_LOOP ( 'NONE', ( #54077, #25609, #51755, #33973 ) ) ;
#45223=CARTESIAN_POINT ( 'NONE',  ( -17.77299844720193533, 11.79293508692305537, -1.500000000000002220 ) ) ;
#45227=CARTESIAN_POINT ( 'NONE',  ( 18.24537196375281312, 10.48796402029766739, -1.500000000000002220 ) ) ;
#45230=CARTESIAN_POINT ( 'NONE',  ( -99.66660779535885695, -25.22553094076996061, 3.606680058317695448 ) ) ;
#45231=CARTESIAN_POINT ( 'NONE',  ( -65.52287095715010423, -24.51254535375846544, 9.355368624242132114 ) ) ;
#45232=CARTESIAN_POINT ( 'NONE',  ( -21.90371867972833542, 1.011951690471867060, -1.500000000000002220 ) ) ;
#45233=PLANE ( 'NONE',  #20364 ) ;
#45235=CARTESIAN_POINT ( 'NONE',  ( -122.5921615827337661, -23.48786465467241769, 11.44779295918253581 ) ) ;
#45237=ADVANCED_FACE ( 'NONE', ( #11336 ), #69461, .T. ) ;
#45238=CARTESIAN_POINT ( 'NONE',  ( -120.5228709571500616, -23.47593901973090524, -1.443836447538996204 ) ) ;
#45239=CARTESIAN_POINT ( 'NONE',  ( -41.62287095715006302, -23.48783264082477729, -1.443836473390071928 ) ) ;
#45240=CARTESIAN_POINT ( 'NONE',  ( -20.43735050632677286, -23.59307763070868447, 9.703205396196684873 ) ) ;
#45241=CARTESIAN_POINT ( 'NONE',  ( 20.09692647535021948, 7.048664716645152595, -1.500000000000002220 ) ) ;
#45242=CARTESIAN_POINT ( 'NONE',  ( -55.62287095715003460, -23.85229601348995132, 10.88205029486210229 ) ) ;
#45244=CARTESIAN_POINT ( 'NONE',  ( -122.5895376238167387, -24.65952944569304961, 1.056160979905702346 ) ) ;
#45245=CARTESIAN_POINT ( 'NONE',  ( -33.49677881317446548, -24.15543982623906771, -0.2315651400026580431 ) ) ;
#45246=CARTESIAN_POINT ( 'NONE',  ( 18.89768980500364037, -12.13386209897132773, -1.500000000000002220 ) ) ;
#45248=CARTESIAN_POINT ( 'NONE',  ( -111.9711973445961917, -25.30561928443788133, 5.929683345795315752 ) ) ;
#45249=ORIENTED_EDGE ( 'NONE', *, *, #63033, .F. ) ;
#45250=CARTESIAN_POINT ( 'NONE',  ( -81.52287095715004739, -24.51387760970724372, 9.387446482453407626 ) ) ;
#45251=CARTESIAN_POINT ( 'NONE',  ( -11.98250242409135780, 15.54504917500377559, 11.49999999999999645 ) ) ;
#45252=CARTESIAN_POINT ( 'NONE',  ( -125.5228709571500616, -25.00158670708909980, 2.256160236439166411 ) ) ;
#45253=CARTESIAN_POINT ( 'NONE',  ( -82.52287095715007581, -24.51283580621453950, 0.6167428607046286926 ) ) ;
#45255=CARTESIAN_POINT ( 'NONE',  ( -88.64271420608834262, -23.48786465467241413, 11.44779295918254469 ) ) ;
#45257=CARTESIAN_POINT ( 'NONE',  ( -100.2069791292054504, -25.25095787178537421, 5.245324546832492274 ) ) ;
#45258=CARTESIAN_POINT ( 'NONE',  ( -26.81181828833286929, -24.64042068939468422, 8.032344318642952175 ) ) ;
#45260=CARTESIAN_POINT ( 'NONE',  ( -5.084378373094740944, 19.06436389234985285, 11.49999999999998934 ) ) ;
#45261=B_SPLINE_CURVE_WITH_KNOTS ( 'NONE', 3,
 ( #20638, #51606, #14523, #45498, #67334, #68824 ),
 .UNSPECIFIED., .F., .F.,
 ( 4, 2, 4 ),
 ( 6.384118678619663671E-06, 0.001386860460828383008, 0.002767336802978146663 ),
 .UNSPECIFIED. ) ;
#45262=ORIENTED_EDGE ( 'NONE', *, *, #92720, .T. ) ;
#45263=PLANE ( 'NONE',  #79674 ) ;
#45268=VERTEX_POINT ( 'NONE', #100033 ) ;
#45269=FACE_OUTER_BOUND ( 'NONE', #12506, .T. ) ;
#45270=CARTESIAN_POINT ( 'NONE',  ( -87.62287095715004170, -24.64965695001468404, 8.947790433994180503 ) ) ;
#45271=CARTESIAN_POINT ( 'NONE',  ( -55.57991759551926947, -24.83618233451449697, 1.606449574219536602 ) ) ;
#45272=CARTESIAN_POINT ( 'NONE',  ( -66.52287095715006160, -24.33832256527049154, 0.1851278514138612330 ) ) ;
#45277=CARTESIAN_POINT ( 'NONE',  ( 18.82558416981596139, 6.732768832687442639, 11.49999999999998934 ) ) ;
#45278=CARTESIAN_POINT ( 'NONE',  ( -127.6228709571500275, -24.33832256526968862, 0.1851278514119955865 ) ) ;
#45279=CARTESIAN_POINT ( 'NONE',  ( -51.04357394935764347, -25.31543073408252553, 4.940877929217665887 ) ) ;
#45280=VERTEX_POINT ( 'NONE', #37661 ) ;
#45284=CARTESIAN_POINT ( 'NONE',  ( -119.5211660777647040, -23.73766607897670866, -1.055555164236450016 ) ) ;
#45285=CARTESIAN_POINT ( 'NONE',  ( -80.50906975063354309, -24.15602025860895807, 10.28564288303536145 ) ) ;
#45286=CARTESIAN_POINT ( 'NONE',  ( -119.6228709571500417, -24.66019654487199730, 8.947790411086121054 ) ) ;
#45287=CARTESIAN_POINT ( 'NONE',  ( -39.50524109486579505, -23.96119346886879597, -0.6495511937832144644 ) ) ;
#45289=CARTESIAN_POINT ( 'NONE',  ( -82.52287095715006160, -24.64965694238407323, 8.947790433994198267 ) ) ;
#45291=EDGE_CURVE ( 'NONE', #85381, #27980, #43788, .T. ) ;
#45293=CARTESIAN_POINT ( 'NONE',  ( -79.62287095715007013, -23.73934037231756733, 11.05740245334329153 ) ) ;
#45294=PLANE ( 'NONE',  #98734 ) ;
#45296=CARTESIAN_POINT ( 'NONE',  ( -8.208445925564873846, -18.52556626786687488, -1.500000000000002220 ) ) ;
#45297=CARTESIAN_POINT ( 'NONE',  ( -69.38672083999394147, -25.31448181975444811, 5.177778959383253721 ) ) ;
#45300=EDGE_CURVE ( 'NONE', #18147, #7077, #82830, .T. ) ;
#45301=CARTESIAN_POINT ( 'NONE',  ( -76.62287095715005592, -23.96127896941631619, -0.6493128931037840390 ) ) ;
#45304=LINE ( 'NONE', #76225, #66451 ) ;
#45305=CARTESIAN_POINT ( 'NONE',  ( -63.62287095715003460, -23.72747288104442021, -1.053458166803663110 ) ) ;
#45306=CARTESIAN_POINT ( 'NONE',  ( -17.50950832565593984, 9.922426906265528146, -1.500000000000002220 ) ) ;
#45307=CARTESIAN_POINT ( 'NONE',  ( 19.97611676871187569, -6.800378171449690257, 11.49999999999999645 ) ) ;
#45310=CARTESIAN_POINT ( 'NONE',  ( -21.88945651911318535, 3.243594245096953710, -1.500000000000002220 ) ) ;
#45311=CARTESIAN_POINT ( 'NONE',  ( 8.954683214801249846, 18.48387022957959047, 11.49999999999998934 ) ) ;
#45313=CARTESIAN_POINT ( 'NONE',  ( -53.62287095715004881, -23.96127896941631619, -0.6493128931037915885 ) ) ;
#45314=ORIENTED_EDGE ( 'NONE', *, *, #35140, .T. ) ;
#45316=EDGE_LOOP ( 'NONE', ( #32736, #86531, #74415, #15102 ) ) ;
#45317=CARTESIAN_POINT ( 'NONE',  ( -99.65705935873248222, -25.15797155923122119, 3.047568788030539544 ) ) ;
#45318=B_SPLINE_SURFACE_WITH_KNOTS ( 'NONE', 3, 3, ( 
 ( #32404, #53752, #70971, #63377 ),
 ( #39515, #46133, #77058, #69960 ),
 ( #445, #62877, #54753, #85688 ),
 ( #50132, #40526, #42030, #95301 ),
 ( #80570, #49640, #25786, #81076 ),
 ( #79572, #65877, #11552, #88695 ),
 ( #65380, #64885, #56761, #96797 ) ),
 .UNSPECIFIED., .F., .F., .F.,
 ( 4, 3, 4 ),
 ( 4, 4 ),
 ( 0.0004766839783820379733, 0.1029713700210895533, 0.2054660560637970590 ),
 ( 0.3195752917425375150, 0.3207354677509840490 ),
 .UNSPECIFIED. ) ;
#45319=CARTESIAN_POINT ( 'NONE',  ( -65.52287095715006160, -24.99132157543083821, 2.256160258750667502 ) ) ;
#45320=ORIENTED_EDGE ( 'NONE', *, *, #76788, .F. ) ;
#45321=ORIENTED_EDGE ( 'NONE', *, *, #68951, .T. ) ;
#45323=CARTESIAN_POINT ( 'NONE',  ( -28.62287095715004881, -23.31954350884483773, -1.443835782653508426 ) ) ;
#45324=CARTESIAN_POINT ( 'NONE',  ( -68.51065382888901922, -23.96169478059712787, 10.65365249895718414 ) ) ;
#45325=CARTESIAN_POINT ( 'NONE',  ( 17.37421522561336928, 11.14841987994331696, -1.500000000000002220 ) ) ;
#45326=ADVANCED_FACE ( 'NONE', ( #90948 ), #51399, .T. ) ;
#45328=CARTESIAN_POINT ( 'NONE',  ( -21.57582672592670292, -1.461774377805347802, 11.49999999999999645 ) ) ;
#45330=FACE_OUTER_BOUND ( 'NONE', #87230, .T. ) ;
#45331=CARTESIAN_POINT ( 'NONE',  ( -96.55620429048337883, -24.64965694238574656, 8.947790433994192938 ) ) ;
#45332=CARTESIAN_POINT ( 'NONE',  ( -14.53400517605410158, 16.95891092046126403, -1.500000000000002220 ) ) ;
#45333=FACE_OUTER_BOUND ( 'NONE', #754, .T. ) ;
#45335=VERTEX_POINT ( 'NONE', #51903 ) ;
#45338=CARTESIAN_POINT ( 'NONE',  ( 19.90007246472742608, 6.374896562862660154, 11.49999999999998934 ) ) ;
#45341=CARTESIAN_POINT ( 'NONE',  ( -67.58377406375005592, -24.51419770103159124, 9.386484678747168076 ) ) ;
#45342=ADVANCED_FACE ( 'NONE', ( #37166 ), #57127, .T. ) ;
#45345=CARTESIAN_POINT ( 'NONE',  ( -50.62287095715005592, -23.84081130438199736, 10.88220057463248658 ) ) ;
#45346=CARTESIAN_POINT ( 'NONE',  ( 21.03498508994548999, -2.205306954651367946, -1.500000000000002220 ) ) ;
#45347=ORIENTED_EDGE ( 'NONE', *, *, #96856, .F. ) ;
#45348=CARTESIAN_POINT ( 'NONE',  ( -112.5228709571500048, -23.95044443724992789, 10.65354141964648882 ) ) ;
#45349=FACE_OUTER_BOUND ( 'NONE', #6390, .T. ) ;
#45350=CARTESIAN_POINT ( 'NONE',  ( 21.79142754302170815, -0.6654467836950721527, -1.500000000000002220 ) ) ;
#45351=CARTESIAN_POINT ( 'NONE',  ( -61.55620429048338593, -23.48786465467241413, 11.44779295918254824 ) ) ;
#45353=DIRECTION ( 'NONE',  ( -3.773278334453079030E-23, 0.9999999999976377785, 2.173523156925979128E-06 ) ) ;
#45354=CARTESIAN_POINT ( 'NONE',  ( -21.62197530259306788, 2.132803791230205359, -1.500000000000002220 ) ) ;
#45356=CARTESIAN_POINT ( 'NONE',  ( 16.41691039316204481, 15.16158741987741365, 11.49999999999999645 ) ) ;
#45357=ORIENTED_EDGE ( 'NONE', *, *, #89436, .T. ) ;
#45359=CARTESIAN_POINT ( 'NONE',  ( -85.62495572383085118, -24.92592662359561473, 8.075495903018000021 ) ) ;
#45363=AXIS2_PLACEMENT_3D ( 'NONE', #91888, #39103, #47231 ) ;
#45364=EDGE_CURVE ( 'NONE', #40713, #67776, #53603, .T. ) ;
#45366=ADVANCED_FACE ( 'NONE', ( #38656 ), #54396, .T. ) ;
#45371=CARTESIAN_POINT ( 'NONE',  ( -13.45780860896912934, -16.40347334334247265, 11.49999999999998934 ) ) ;
#45373=CARTESIAN_POINT ( 'NONE',  ( -79.14729083585920932, -25.03138132657652193, 6.795304888836573021 ) ) ;
#45377=CARTESIAN_POINT ( 'NONE',  ( -17.66094656686658482, 7.961706694365092041, -1.500000000000002220 ) ) ;
#45378=EDGE_CURVE ( 'NONE', #64588, #32345, #63522, .T. ) ;
#45379=CARTESIAN_POINT ( 'NONE',  ( -39.98858864963047210, -25.03707806782366418, 7.590868867492675420 ) ) ;
#45380=ORIENTED_EDGE ( 'NONE', *, *, #63488, .F. ) ;
#45381=CARTESIAN_POINT ( 'NONE',  ( 19.33761327413411024, 2.027444641817329973, 11.49999999999999645 ) ) ;
#45382=CARTESIAN_POINT ( 'NONE',  ( -115.5228709571500616, -23.48786465467241769, 11.44779295918253759 ) ) ;
#45383=ORIENTED_EDGE ( 'NONE', *, *, #28629, .F. ) ;
#45385=CARTESIAN_POINT ( 'NONE',  ( -32.62287095715004881, -29.50250243563736774, 8.947779886222150481 ) ) ;
#45386=CARTESIAN_POINT ( 'NONE',  ( -59.52287095715004739, -24.51387760970726148, 9.387446482453434271 ) ) ;
#45388=CARTESIAN_POINT ( 'NONE',  ( -19.13235715846047214, 4.354950445902704637, -1.500000000000002220 ) ) ;
#45391=CARTESIAN_POINT ( 'NONE',  ( -13.10987527212420645, -17.12674121770768920, -1.500000000000002220 ) ) ;
#45392=CARTESIAN_POINT ( 'NONE',  ( -33.52640019870900545, -24.66019654487198665, 8.947790411086133489 ) ) ;
#45393=CARTESIAN_POINT ( 'NONE',  ( -40.52320638232922079, -24.92564183028978775, 1.928384488918254203 ) ) ;
#45394=CARTESIAN_POINT ( 'NONE',  ( -100.4008197971955667, -25.27473221760678257, 3.294680443612905574 ) ) ;
#45395=CARTESIAN_POINT ( 'NONE',  ( -22.84742429131147645, -2.885717679200183738, -1.500000000000002220 ) ) ;
#45397=DIRECTION ( 'NONE',  ( -0.000000000000000000, 2.173523156925979552E-06, -0.9999999999976378895 ) ) ;
#45399=CARTESIAN_POINT ( 'NONE',  ( -14.30055291515510518, -14.21740073472259525, 11.49999999999999645 ) ) ;
#45400=CARTESIAN_POINT ( 'NONE',  ( -109.0459178056501486, -25.28814249556381810, 3.663604978347184016 ) ) ;
#45404=DIRECTION ( 'NONE',  ( -3.773278334453079618E-23, 0.9999999999976377785, 2.173523156925979975E-06 ) ) ;
#45405=CARTESIAN_POINT ( 'NONE',  ( 15.68239283413728735, 12.23493734220040530, 11.49999999999998934 ) ) ;
#45407=CARTESIAN_POINT ( 'NONE',  ( 19.71268880909926580, -1.816447362451163450, -1.500000000000002220 ) ) ;
#45408=CARTESIAN_POINT ( 'NONE',  ( -126.5222601503578943, -23.48786465467241769, 11.44779295918253759 ) ) ;
#45409=CARTESIAN_POINT ( 'NONE',  ( -123.6228709571500559, -23.47596703998600631, 11.44779298504227860 ) ) ;
#45410=CARTESIAN_POINT ( 'NONE',  ( -66.62287095715005592, -23.47593901973091235, -1.443836447539006196 ) ) ;
#45411=CARTESIAN_POINT ( 'NONE',  ( 4.478411676025833010, -20.21887007069289766, 11.49999999999999645 ) ) ;
#45412=CARTESIAN_POINT ( 'NONE',  ( -58.52287095715005449, -23.72747288104470087, -1.053458166803226570 ) ) ;
#45414=CARTESIAN_POINT ( 'NONE',  ( -79.62287095715004170, -23.47596703998600631, 11.44779298504227860 ) ) ;
#45415=CARTESIAN_POINT ( 'NONE',  ( 20.46598465274837864, -9.837531852206524263, 11.49999999999999645 ) ) ;
#45418=LINE ( 'NONE', #36306, #59255 ) ;
#45419=CARTESIAN_POINT ( 'NONE',  ( -33.58953762381673158, -24.66019654487199020, 8.947790411086131712 ) ) ;
#45422=EDGE_CURVE ( 'NONE', #57540, #66877, #42638, .T. ) ;
#45423=CARTESIAN_POINT ( 'NONE',  ( -18.21026628907936029, 8.684577975296603469, -1.500000000000002220 ) ) ;
#45424=DIRECTION ( 'NONE',  ( 1.000000000000000000, 3.773278334444167608E-23, 8.201307833595939069E-29 ) ) ;
#45425=EDGE_CURVE ( 'NONE', #21744, #5489, #78907, .T. ) ;
#45426=CARTESIAN_POINT ( 'NONE',  ( -52.52287095715009002, -23.72773821059535848, 11.05748984161097503 ) ) ;
#45428=ORIENTED_EDGE ( 'NONE', *, *, #5110, .T. ) ;
#45430=EDGE_CURVE ( 'NONE', #32236, #11225, #61352, .T. ) ;
#45433=CARTESIAN_POINT ( 'NONE',  ( 22.81499323874321661, -2.031749852351878882, -1.500000000000002220 ) ) ;
#45434=DIRECTION ( 'NONE',  ( 0.000000000000000000, -0.9999999999976377785, -2.173523156925979975E-06 ) ) ;
#45436=CARTESIAN_POINT ( 'NONE',  ( 12.90450488963236353, -17.39418326053592168, -1.500000000000002220 ) ) ;
#45437=PLANE ( 'NONE',  #38258 ) ;
#45439=CARTESIAN_POINT ( 'NONE',  ( -18.74228827200876779, -9.293929619069025705, 11.49999999999999645 ) ) ;
#45443=CARTESIAN_POINT ( 'NONE',  ( 2.959355296939036872, -21.81356824310248399, -1.500000000000002220 ) ) ;
#45445=CARTESIAN_POINT ( 'NONE',  ( -105.5608698559539391, -23.48786465467241769, 11.44779295918254114 ) ) ;
#45446=CARTESIAN_POINT ( 'NONE',  ( -28.45645220296530908, -24.79700262693759782, 7.353600621000675908 ) ) ;
#45447=VERTEX_POINT ( 'NONE', #22754 ) ;
#45449=CARTESIAN_POINT ( 'NONE',  ( -90.59981717707987059, -23.85049219812686161, 10.88485053497527488 ) ) ;
#45451=CARTESIAN_POINT ( 'NONE',  ( -72.59232271956842908, -24.15620529776628089, 10.23563542870660825 ) ) ;
#45452=ORIENTED_EDGE ( 'NONE', *, *, #22489, .T. ) ;
#45454=CARTESIAN_POINT ( 'NONE',  ( -71.62363258555255641, -24.66019654487199730, 8.947790411086113949 ) ) ;
#45455=LINE ( 'NONE', #37339, #38956 ) ;
#45456=CARTESIAN_POINT ( 'NONE',  ( -57.50860782142563465, -23.96119346886880663, -0.6495511937832122440 ) ) ;
#45457=CARTESIAN_POINT ( 'NONE',  ( 1.259202695315177589, 20.44674571593545664, -1.500000000000002220 ) ) ;
#45458=EDGE_CURVE ( 'NONE', #59957, #80599, #39021, .T. ) ;
#45461=CARTESIAN_POINT ( 'NONE',  ( -30.64427850938831099, -23.56000036390796382, 11.50200000000000067 ) ) ;
#45464=CARTESIAN_POINT ( 'NONE',  ( -51.62287095715005592, -24.64965695001468404, 8.947790433994185832 ) ) ;
#45465=EDGE_CURVE ( 'NONE', #44470, #65117, #84667, .T. ) ;
#45467=CARTESIAN_POINT ( 'NONE',  ( -104.5228709571500758, -23.47593901973090524, -1.443836447538996204 ) ) ;
#45468=CARTESIAN_POINT ( 'NONE',  ( -29.47349813062140100, -25.26247812443174467, 7.035455039352441098 ) ) ;
#45469=CARTESIAN_POINT ( 'NONE',  ( 20.50115541507891948, 3.495740877612329101, -1.500000000000002220 ) ) ;
#45470=VERTEX_POINT ( 'NONE', #60853 ) ;
#45471=CARTESIAN_POINT ( 'NONE',  ( -54.62287095715003460, -24.33832256526968507, 0.1851278514119833740 ) ) ;
#45473=B_SPLINE_CURVE_WITH_KNOTS ( 'NONE', 3,
 ( #81384, #58067, #48947, #79875, #72284, #2776 ),
 .UNSPECIFIED., .F., .F.,
 ( 4, 2, 4 ),
 ( 1.570755371633934808E-05, 0.001396183895866087103, 0.002776660238015835145 ),
 .UNSPECIFIED. ) ;
#45475=VERTEX_POINT ( 'NONE', #76539 ) ;
#45476=ORIENTED_EDGE ( 'NONE', *, *, #94165, .F. ) ;
#45479=CARTESIAN_POINT ( 'NONE',  ( -76.52287095715007581, -24.64965694238408034, 8.947790433994198267 ) ) ;
#45480=CARTESIAN_POINT ( 'NONE',  ( -51.52287095715006870, -24.65952944569304606, 1.056160979905693686 ) ) ;
#45481=B_SPLINE_CURVE_WITH_KNOTS ( 'NONE', 3,
 ( #51166, #74494, #27826, #97338 ),
 .UNSPECIFIED., .F., .F.,
 ( 4, 4 ),
 ( 0.000000000000000000, 9.999999999998897304E-05 ),
 .UNSPECIFIED. ) ;
#45482=CARTESIAN_POINT ( 'NONE',  ( -92.51846257638729298, -23.73791477778912196, 11.05961554403170588 ) ) ;
#45483=CARTESIAN_POINT ( 'NONE',  ( -73.62287095715007013, -24.66019654487199020, 8.947790411086131712 ) ) ;
#45484=CARTESIAN_POINT ( 'NONE',  ( -7.320055889550622474, -20.87099576385019972, 11.49999999999999645 ) ) ;
#45485=ORIENTED_EDGE ( 'NONE', *, *, #76896, .T. ) ;
#45487=CARTESIAN_POINT ( 'NONE',  ( -22.13905560727926414, 4.690293145198261904, 11.49999999999998934 ) ) ;
#45488=EDGE_CURVE ( 'NONE', #27742, #41495, #83757, .T. ) ;
#45489=CARTESIAN_POINT ( 'NONE',  ( -87.58953762381671027, -23.47593901973091235, -1.443836447539002865 ) ) ;
#45490=ORIENTED_EDGE ( 'NONE', *, *, #63140, .F. ) ;
#45491=VERTEX_POINT ( 'NONE', #90790 ) ;
#45492=CARTESIAN_POINT ( 'NONE',  ( -122.6228709571500417, -23.48786465467242124, 11.44779295918253759 ) ) ;
#45494=B_SPLINE_CURVE_WITH_KNOTS ( 'NONE', 3,
 ( #76154, #44729, #22357, #84273, #45231, #83278, #38101, #76647 ),
 .UNSPECIFIED., .F., .F.,
 ( 4, 2, 2, 4 ),
 ( -0.001240355328176878311, -0.0002398155169399597986, 0.0007607242942969587134, 0.002761803916770787931 ),
 .UNSPECIFIED. ) ;
#45495=CARTESIAN_POINT ( 'NONE',  ( 6.436487395234643749, 19.08016507665710648, 11.49999999999998934 ) ) ;
#45498=CARTESIAN_POINT ( 'NONE',  ( -126.5228709571501184, -24.34917612406837861, 0.1852690917426611239 ) ) ;
#45499=CARTESIAN_POINT ( 'NONE',  ( -11.77839732991513166, 18.97803183815481987, -1.500000000000002220 ) ) ;
#45500=ORIENTED_EDGE ( 'NONE', *, *, #21910, .T. ) ;
#45501=EDGE_LOOP ( 'NONE', ( #11200, #25567, #71331, #48089 ) ) ;
#45502=DIRECTION ( 'NONE',  ( 3.773278334444167608E-23, -1.000000000000000000, 0.000000000000000000 ) ) ;
#45503=CARTESIAN_POINT ( 'NONE',  ( -124.5228709571500616, -29.50250243563736774, 8.947779886222134493 ) ) ;
#45506=DIRECTION ( 'NONE',  ( -1.000000000000000000, -3.773278334444166432E-23, -8.201307841325785021E-29 ) ) ;
#45508=CARTESIAN_POINT ( 'NONE',  ( 3.395600993332231532, 19.23619202488179525, 11.49999999999998934 ) ) ;
#45511=CARTESIAN_POINT ( 'NONE',  ( -5.860608850286626925, 20.67097946995454905, -1.500000000000002220 ) ) ;
#45513=PLANE ( 'NONE',  #53555 ) ;
#45515=CARTESIAN_POINT ( 'NONE',  ( -9.520747347383798243, -20.79447232172871907, -1.500000000000002220 ) ) ;
#45517=CARTESIAN_POINT ( 'NONE',  ( -96.55228293290541330, -24.15620529776628445, 10.23563542870660115 ) ) ;
#45519=CARTESIAN_POINT ( 'NONE',  ( 12.72590371223024697, 15.41468647733915809, 11.49999999999999645 ) ) ;
#45520=PLANE ( 'NONE',  #97096 ) ;
#45521=CARTESIAN_POINT ( 'NONE',  ( -74.51177717695108527, -23.96169478059713498, 10.65365249895717881 ) ) ;
#45524=DIRECTION ( 'NONE',  ( -1.000000000000000000, -3.773278334444166432E-23, -8.201307841325785021E-29 ) ) ;
#45526=CARTESIAN_POINT ( 'NONE',  ( -1.994712787082457472, 21.64621699974126656, -1.500000000000002220 ) ) ;
#45527=FACE_OUTER_BOUND ( 'NONE', #70523, .T. ) ;
#45528=CARTESIAN_POINT ( 'NONE',  ( -6.824658503225996320, 18.35159230250476270, -1.500000000000002220 ) ) ;
#45529=CARTESIAN_POINT ( 'NONE',  ( -74.52287095715007581, -29.50248528299804818, 1.056150453629036701 ) ) ;
#45530=B_SPLINE_CURVE_WITH_KNOTS ( 'NONE', 3,
 ( #10339, #41807, #49422, #18450, #50908, #26573, #57534, #26061, #42805, #3249, #33681, #43299, #4230, #88972 ),
 .UNSPECIFIED., .F., .F.,
 ( 4, 2, 2, 2, 2, 2, 4 ),
 ( 7.059813062317230268E-18, 0.0001563035440846473692, 0.0003126070881692876910, 0.0006252141763385689853, 0.0009378212645078503338, 0.001094124808592491713, 0.001250428352677132766 ),
 .UNSPECIFIED. ) ;
#45532=LINE ( 'NONE', #20676, #56454 ) ;
#45534=CARTESIAN_POINT ( 'NONE',  ( -16.44861368136865920, 12.28130381464353782, 11.49999999999999645 ) ) ;
#45535=CARTESIAN_POINT ( 'NONE',  ( -121.5228709571500616, -29.50248528299804818, 1.056150453629045360 ) ) ;
#45536=PLANE ( 'NONE',  #46472 ) ;
#45537=ADVANCED_FACE ( 'NONE', ( #68453 ), #44617, .T. ) ;
#45539=CARTESIAN_POINT ( 'NONE',  ( -72.52287095715009002, -24.51283580621365488, 0.6167428607019659337 ) ) ;
#45541=CARTESIAN_POINT ( 'NONE',  ( -90.62287095715004170, -23.48786465467241058, 11.44779295918254469 ) ) ;
#45542=EDGE_CURVE ( 'NONE', #6180, #43572, #28061, .T. ) ;
#45543=CARTESIAN_POINT ( 'NONE',  ( -69.62287095715005592, -24.64965695001468404, 8.947790433994184056 ) ) ;
#45544=CARTESIAN_POINT ( 'NONE',  ( -85.52287095715004739, -24.52232992886361629, 0.6492154411906000400 ) ) ;
#45545=EDGE_CURVE ( 'NONE', #59154, #5489, #5052, .T. ) ;
#45546=DIRECTION ( 'NONE',  ( 0.000000000000000000, 0.9999999999976377785, 2.173523156925979975E-06 ) ) ;
#45548=CARTESIAN_POINT ( 'NONE',  ( 6.910522817300494225, 22.03692736239173300, 11.49999999999999645 ) ) ;
#45549=CARTESIAN_POINT ( 'NONE',  ( -6.082769120682566921, -21.99330073093985405, -1.500000000000002220 ) ) ;
#45550=CARTESIAN_POINT ( 'NONE',  ( -110.6352833674019820, -23.48786465467241769, 11.44779295918253759 ) ) ;
#45551=EDGE_CURVE ( 'NONE', #86024, #53534, #98309, .T. ) ;
#45553=CARTESIAN_POINT ( 'NONE',  ( -85.58953762381669605, -24.99156044556120193, 7.747789690856343725 ) ) ;
#45554=PLANE ( 'NONE',  #49608 ) ;
#45556=CARTESIAN_POINT ( 'NONE',  ( -99.64934318012689118, -25.31582198417827811, 4.927356293751860683 ) ) ;
#45558=CARTESIAN_POINT ( 'NONE',  ( 20.64021973274467570, 7.317367941133321452, -1.500000000000002220 ) ) ;
#45559=CARTESIAN_POINT ( 'NONE',  ( -58.62287095715004881, -23.48783264082478439, -1.443836473390069264 ) ) ;
#45561=CARTESIAN_POINT ( 'NONE',  ( -77.62287095715011276, -24.51283580621365132, 0.6167428607019761477 ) ) ;
#45562=CARTESIAN_POINT ( 'NONE',  ( -105.5228709571500758, -29.50250786944525672, 11.44777988621622988 ) ) ;
#45564=CARTESIAN_POINT ( 'NONE',  ( -122.6228709571500985, -24.35013146730204525, 9.818937971375095941 ) ) ;
#45566=B_SPLINE_CURVE_WITH_KNOTS ( 'NONE', 3,
 ( #43621, #50738, #90289, #68452, #35996, #51732, #28887, #97885, #98889, #97401, #27887, #29382, #44119, #74561 ),
 .UNSPECIFIED., .F., .F.,
 ( 4, 2, 2, 2, 2, 2, 4 ),
 ( 3.469446951953614189E-18, 0.0002365416005296795297, 0.0004730832010593555900, 0.0007096248015890316502, 0.0009461664021187077105, 0.001419249603178059831, 0.001892332804237411951 ),
 .UNSPECIFIED. ) ;
#45567=CARTESIAN_POINT ( 'NONE',  ( 16.92567061652012228, 11.46397006495115534, -1.500000000000002220 ) ) ;
#45569=ORIENTED_EDGE ( 'NONE', *, *, #25017, .F. ) ;
#45570=EDGE_LOOP ( 'NONE', ( #27763, #21139, #68150, #94535 ) ) ;
#45571=EDGE_LOOP ( 'NONE', ( #89125, #37335, #11152, #98838 ) ) ;
#45572=CARTESIAN_POINT ( 'NONE',  ( -21.01138170180016118, -9.542296329091309204, -1.500000000000002220 ) ) ;
#45573=CARTESIAN_POINT ( 'NONE',  ( -35.52287095715005449, -23.48783264083451883, -1.443836473374936258 ) ) ;
#45574=CARTESIAN_POINT ( 'NONE',  ( 12.15850541088210868, 16.18036119754114566, -1.500000000000002220 ) ) ;
#45575=EDGE_LOOP ( 'NONE', ( #93518, #72798, #31987, #77263 ) ) ;
#45576=CARTESIAN_POINT ( 'NONE',  ( -29.26507481595814752, -25.20890896920636592, 5.848370260082334404 ) ) ;
#45577=CARTESIAN_POINT ( 'NONE',  ( -127.6228709571500559, -24.64965695001469115, 8.947790433994173398 ) ) ;
#45579=CARTESIAN_POINT ( 'NONE',  ( -47.55620429048338593, -23.48783264082478084, -1.443836473390070596 ) ) ;
#45580=CARTESIAN_POINT ( 'NONE',  ( -99.51410621055458705, -24.15620529776628800, 10.23563542870660115 ) ) ;
#45581=CARTESIAN_POINT ( 'NONE',  ( 15.63241172484657682, -14.69700884395465934, 11.49999999999999645 ) ) ;
#45582=ORIENTED_EDGE ( 'NONE', *, *, #16502, .T. ) ;
#45583=CARTESIAN_POINT ( 'NONE',  ( -113.6228709571500417, -23.72747288104442021, -1.053458166803661777 ) ) ;
#45587=CARTESIAN_POINT ( 'NONE',  ( 8.970943996638910178, -18.66293075132952950, 11.49999999999998934 ) ) ;
#45589=ORIENTED_EDGE ( 'NONE', *, *, #98010, .T. ) ;
#45590=CARTESIAN_POINT ( 'NONE',  ( -28.62167455042580499, -23.33138160483529688, -1.443835813551990865 ) ) ;
#45593=CARTESIAN_POINT ( 'NONE',  ( -65.59221808990133695, -24.40034930558990922, 0.3402023900116040167 ) ) ;
#45594=CARTESIAN_POINT ( 'NONE',  ( -9.458160343781703006, 19.84743614482962926, 11.49999999999999645 ) ) ;
#45595=CARTESIAN_POINT ( 'NONE',  ( -105.6228709571500417, -29.50249982740957577, 7.747779886224967605 ) ) ;
#45596=CARTESIAN_POINT ( 'NONE',  ( 6.619388286264371146, -21.57091762011834390, 11.49999999999998934 ) ) ;
#45597=CARTESIAN_POINT ( 'NONE',  ( -13.85205798638896901, 15.75786377350088507, -1.500000000000002220 ) ) ;
#45598=CARTESIAN_POINT ( 'NONE',  ( -70.35895856474229504, -25.30161620421289470, 5.313173632321669615 ) ) ;
#45603=CARTESIAN_POINT ( 'NONE',  ( -88.52287095715010423, -23.72773821059536914, 11.05748984161097503 ) ) ;
#45605=CARTESIAN_POINT ( 'NONE',  ( -15.55086147716002110, 14.89234021980106881, -1.500000000000002220 ) ) ;
#45606=EDGE_CURVE ( 'NONE', #40077, #54069, #23298, .T. ) ;
#45607=DIRECTION ( 'NONE',  ( 0.000000000000000000, 0.9999999999976377785, 2.173523156925979128E-06 ) ) ;
#45608=VERTEX_POINT ( 'NONE', #94278 ) ;
#45609=CARTESIAN_POINT ( 'NONE',  ( -19.39432879369159224, 8.380699159679657839, -1.500000000000002220 ) ) ;
#45611=CARTESIAN_POINT ( 'NONE',  ( -64.55954162791702799, -23.73766607897670156, -1.055555164236459564 ) ) ;
#45612=CARTESIAN_POINT ( 'NONE',  ( -100.5228709571500616, -25.00158670708909625, 2.256160236439166411 ) ) ;
#45613=CARTESIAN_POINT ( 'NONE',  ( -46.52287095715006160, -29.50250786944525672, 11.44777988621624054 ) ) ;
#45614=CARTESIAN_POINT ( 'NONE',  ( -123.6228709571500559, -23.48783264082478794, -1.443836473390058606 ) ) ;
#45615=CARTESIAN_POINT ( 'NONE',  ( 4.260453091581613450, -21.75001586557718980, -1.500000000000002220 ) ) ;
#45616=CARTESIAN_POINT ( 'NONE',  ( -71.62363249165781554, -24.65952944569304961, 1.056160979905700570 ) ) ;
#45618=CARTESIAN_POINT ( 'NONE',  ( -51.52812418322009336, -25.31633154934941743, 5.264378407383865088 ) ) ;
#45621=B_SPLINE_CURVE_WITH_KNOTS ( 'NONE', 3,
 ( #25342, #87239, #55813, #24839 ),
 .UNSPECIFIED., .F., .F.,
 ( 4, 4 ),
 ( 0.000000000000000000, 0.0001002978970083000140 ),
 .UNSPECIFIED. ) ;
#45622=CARTESIAN_POINT ( 'NONE',  ( -97.52287095715006160, -23.47596703998600631, 11.44779298504228215 ) ) ;
#45623=CARTESIAN_POINT ( 'NONE',  ( 17.65527434030279252, -8.155491144718855168, 11.49999999999998934 ) ) ;
#45624=CARTESIAN_POINT ( 'NONE',  ( -1.242826169824672977, 21.35102975155811222, 11.49999999999998934 ) ) ;
#45625=CARTESIAN_POINT ( 'NONE',  ( -64.58953762381673869, -24.65952944569304250, 1.056160979905695907 ) ) ;
#45627=AXIS2_PLACEMENT_3D ( 'NONE', #8322, #86446, #40276 ) ;
#45629=CARTESIAN_POINT ( 'NONE',  ( -129.5228709571500758, -23.47593901973090524, -1.443836447538996204 ) ) ;
#45630=EDGE_CURVE ( 'NONE', #58910, #82905, #77544, .T. ) ;
#45631=CARTESIAN_POINT ( 'NONE',  ( -16.08347380570801377, -15.98036338121420030, -1.500000000000002220 ) ) ;
#45632=ORIENTED_EDGE ( 'NONE', *, *, #29676, .T. ) ;
#45634=CARTESIAN_POINT ( 'NONE',  ( -102.5562042904834072, -24.64965694238575011, 8.947790433994196491 ) ) ;
#45635=CARTESIAN_POINT ( 'NONE',  ( -8.418173371947181849, -17.93405594323863284, 11.49999999999999645 ) ) ;
#45640=CARTESIAN_POINT ( 'NONE',  ( 20.55956107658784404, -6.795330137259728787, -1.500000000000002220 ) ) ;
#45641=LINE ( 'NONE', #35541, #39921 ) ;
#45642=CARTESIAN_POINT ( 'NONE',  ( 13.61561175257155298, 13.87280521877887018, -1.500000000000002220 ) ) ;
#45644=CARTESIAN_POINT ( 'NONE',  ( -129.5228709571500758, -24.50321055353805377, 9.387540953477515160 ) ) ;
#45645=CARTESIAN_POINT ( 'NONE',  ( 16.01007288495529224, -11.65062672332236104, -1.500000000000002220 ) ) ;
#45649=CARTESIAN_POINT ( 'NONE',  ( 2.303441031721801480, -20.17751241584783628, 11.49999999999999645 ) ) ;
#45650=CARTESIAN_POINT ( 'NONE',  ( -40.62287095715004170, -29.50249982740957577, 7.747779886224967605 ) ) ;
#45652=B_SPLINE_CURVE_WITH_KNOTS ( 'NONE', 3,
 ( #78092, #62911, #70503, #55795, #61900, #992 ),
 .UNSPECIFIED., .F., .F.,
 ( 4, 2, 4 ),
 ( 1.570887131794333942E-05, 0.001396322306279758904, 0.002776935741241574537 ),
 .UNSPECIFIED. ) ;
#45654=DIRECTION ( 'NONE',  ( -3.773278334444166432E-23, 1.000000000000000000, 0.000000000000000000 ) ) ;
#45656=CARTESIAN_POINT ( 'NONE',  ( -48.95379770480546711, -25.31601981760315923, 5.698183519111846174 ) ) ;
#45657=DIRECTION ( 'NONE',  ( -3.773278334453079618E-23, 0.9999999999976377785, 2.173523156925979975E-06 ) ) ;
#45659=CARTESIAN_POINT ( 'NONE',  ( -18.95788008782500356, -6.583919088883305015, -1.500000000000002220 ) ) ;
#45661=EDGE_CURVE ( 'NONE', #52812, #66746, #16652, .T. ) ;
#45664=EDGE_CURVE ( 'NONE', #38848, #79772, #79558, .T. ) ;
#45665=CARTESIAN_POINT ( 'NONE',  ( -4.681240387505234857, -22.43558246840685300, 11.49999999999999645 ) ) ;
#45666=CARTESIAN_POINT ( 'NONE',  ( 20.46598465274837864, -9.837531852206524263, -1.500000000000002220 ) ) ;
#45669=CARTESIAN_POINT ( 'NONE',  ( -28.52287095715006870, -24.35176667652165250, 0.6166262579151312595 ) ) ;
#45670=CARTESIAN_POINT ( 'NONE',  ( -38.63477338751106771, -24.35071581493542325, 9.817618358456030592 ) ) ;
#45671=ADVANCED_FACE ( 'NONE', ( #54240 ), #54085, .T. ) ;
#45673=CARTESIAN_POINT ( 'NONE',  ( -117.6228709571500559, -23.47596703998600631, 11.44779298504227683 ) ) ;
#45677=CARTESIAN_POINT ( 'NONE',  ( -19.36681041099238598, 6.328833669845586485, -1.500000000000002220 ) ) ;
#45678=EDGE_LOOP ( 'NONE', ( #68093, #26482, #90087, #6715 ) ) ;
#45680=CARTESIAN_POINT ( 'NONE',  ( 21.75294195941402364, -7.338126679257295670, -1.500000000000002220 ) ) ;
#45681=CARTESIAN_POINT ( 'NONE',  ( -62.52287095715006160, -29.50250786944525672, 11.44777988621623876 ) ) ;
#45683=PLANE ( 'NONE',  #3970 ) ;
#45684=CARTESIAN_POINT ( 'NONE',  ( -116.5228709571500900, -24.51387760970725793, 9.387446482453407626 ) ) ;
#45685=CARTESIAN_POINT ( 'NONE',  ( -51.54737341646723792, -24.15620529776627734, 10.23563542870660470 ) ) ;
#45686=CARTESIAN_POINT ( 'NONE',  ( 14.73992482348874411, 15.29747818672187165, 11.49999999999999645 ) ) ;
#45688=VERTEX_POINT ( 'NONE', #27771 ) ;
#45689=CARTESIAN_POINT ( 'NONE',  ( 5.796264663052079769, -21.44337444023769379, 11.49999999999998934 ) ) ;
#45691=CARTESIAN_POINT ( 'NONE',  ( -20.60669311552257810, 0.8253496925510150906, 11.49999999999998934 ) ) ;
#45692=B_SPLINE_CURVE_WITH_KNOTS ( 'NONE', 3,
 ( #60190, #98219, #44960, #6386, #35840, #5387, #12498, #4894 ),
 .UNSPECIFIED., .F., .F.,
 ( 4, 2, 2, 4 ),
 ( 0.000000000000000000, 0.002001079623178224094, 0.003001619434767337658, 0.004002159246356451656 ),
 .UNSPECIFIED. ) ;
#45696=CARTESIAN_POINT ( 'NONE',  ( -40.25280366610014227, -25.12199515523669291, 2.840616586787004128 ) ) ;
#45697=ORIENTED_EDGE ( 'NONE', *, *, #55908, .F. ) ;
#45698=CARTESIAN_POINT ( 'NONE',  ( -51.62287095715005592, -24.66019654487199020, 8.947790411086135265 ) ) ;
#45699=ORIENTED_EDGE ( 'NONE', *, *, #22751, .F. ) ;
#45700=CARTESIAN_POINT ( 'NONE',  ( -39.52287095715006870, -24.64965694238406613, 8.947790433994205372 ) ) ;
#45701=CARTESIAN_POINT ( 'NONE',  ( -45.62287095715004881, -24.99132157543083821, 2.256160258750667502 ) ) ;
#45702=CARTESIAN_POINT ( 'NONE',  ( 20.70993026999094511, 1.908435391604796028, -1.500000000000002220 ) ) ;
#45703=CARTESIAN_POINT ( 'NONE',  ( 19.81658424304261246, 9.080307684375437560, 11.49999999999999645 ) ) ;
#45704=CARTESIAN_POINT ( 'NONE',  ( -39.97032894598978459, -25.19873439044615893, 3.393671681319915034 ) ) ;
#45705=CARTESIAN_POINT ( 'NONE',  ( -99.28744282076259253, -25.12404174411991775, 7.096701639951624507 ) ) ;
#45706=CARTESIAN_POINT ( 'NONE',  ( -16.74552829020559130, -14.98668287627115170, -1.500000000000002220 ) ) ;
#45707=CARTESIAN_POINT ( 'NONE',  ( -50.56373716527822637, -25.26334748840130828, 4.723080157104919685 ) ) ;
#45710=B_SPLINE_CURVE_WITH_KNOTS ( 'NONE', 3,
 ( #99266, #76419, #37878, #44499 ),
 .UNSPECIFIED., .F., .F.,
 ( 4, 4 ),
 ( 0.000000000000000000, 9.999999999998897304E-05 ),
 .UNSPECIFIED. ) ;
#45711=CARTESIAN_POINT ( 'NONE',  ( -80.88924702628075636, -25.30869131066464561, 4.592921213095906730 ) ) ;
#45713=CARTESIAN_POINT ( 'NONE',  ( -101.9507253916653440, -25.24282061761981666, 6.236250683194342059 ) ) ;
#45715=ORIENTED_EDGE ( 'NONE', *, *, #88499, .F. ) ;
#45716=ORIENTED_EDGE ( 'NONE', *, *, #85648, .F. ) ;
#45717=EDGE_CURVE ( 'NONE', #91001, #83268, #25773, .T. ) ;
#45719=CARTESIAN_POINT ( 'NONE',  ( -1.966620079519992181, -21.27258529651320274, -1.500000000000002220 ) ) ;
#45721=CARTESIAN_POINT ( 'NONE',  ( 2.700122536338566359, 20.86363338933649558, -1.500000000000002220 ) ) ;
#45722=CARTESIAN_POINT ( 'NONE',  ( -30.47816396153159602, -24.83083109926283072, 1.633466014234818076 ) ) ;
#45725=CARTESIAN_POINT ( 'NONE',  ( -21.86317675896206225, -2.224439152981679602, -1.500000000000002220 ) ) ;
#45726=CARTESIAN_POINT ( 'NONE',  ( -87.63524930070781238, -23.96119346886882084, -0.6495511937831871530 ) ) ;
#45729=B_SPLINE_CURVE_WITH_KNOTS ( 'NONE', 3,
 ( #92928, #54388, #77695, #92431 ),
 .UNSPECIFIED., .F., .F.,
 ( 4, 4 ),
 ( 0.9663008150836682741, 0.9998940316929132432 ),
 .UNSPECIFIED. ) ;
#45731=CARTESIAN_POINT ( 'NONE',  ( -128.5228709571499621, -23.73907113217699560, -1.053371485780730143 ) ) ;
#45732=CARTESIAN_POINT ( 'NONE',  ( -30.58080474561622353, -25.30588374461880008, 5.002395802403317049 ) ) ;
#45733=CARTESIAN_POINT ( 'NONE',  ( -3.120219904758775975, 21.05623772282662998, 11.49999999999998934 ) ) ;
#45734=PLANE ( 'NONE',  #64531 ) ;
#45735=CARTESIAN_POINT ( 'NONE',  ( -107.5222081683197786, -23.48786465467241769, 11.44779295918253936 ) ) ;
#45737=DIRECTION ( 'NONE',  ( -3.773278334453079030E-23, 0.9999999999976377785, 2.173523156925979128E-06 ) ) ;
#45739=CARTESIAN_POINT ( 'NONE',  ( 12.90280524143238594, -18.44629484376132922, -1.500000000000002220 ) ) ;
#45740=B_SPLINE_SURFACE_WITH_KNOTS ( 'NONE', 3, 3, ( 
 ( #11139, #71551, #42109, #26866 ),
 ( #88776, #50210, #11630, #2044 ),
 ( #32986, #64462, #42608, #65955 ),
 ( #48724, #95376, #73544, #4037 ),
 ( #25864, #14122, #6018, #60331 ),
 ( #51705, #6525, #75518, #27861 ),
 ( #12633, #44591, #22227, #36973 ) ),
 .UNSPECIFIED., .F., .F., .F.,
 ( 4, 3, 4 ),
 ( 4, 4 ),
 ( 0.7945040050992242531, 0.8970133687736503436, 0.9995227324480764342 ),
 ( 0.5696387503446669331, 0.5709144579475504688 ),
 .UNSPECIFIED. ) ;
#45741=PLANE ( 'NONE',  #50671 ) ;
#45743=CARTESIAN_POINT ( 'NONE',  ( -99.77167476857428596, -25.07038923500906691, 7.433068779553578587 ) ) ;
#45744=CARTESIAN_POINT ( 'NONE',  ( -8.122062702759739850, 17.86989387945112995, 11.49999999999999645 ) ) ;
#45745=LINE ( 'NONE', #69077, #1746 ) ;
#45746=B_SPLINE_CURVE_WITH_KNOTS ( 'NONE', 3,
 ( #92232, #84122, #93229, #76496 ),
 .UNSPECIFIED., .F., .F.,
 ( 4, 4 ),
 ( 0.3607576081775127896, 0.3697640394496283234 ),
 .UNSPECIFIED. ) ;
#45748=ORIENTED_EDGE ( 'NONE', *, *, #43892, .T. ) ;
#45749=CARTESIAN_POINT ( 'NONE',  ( -88.54317737591240700, -24.66019654487199730, 8.947790411086115725 ) ) ;
#45750=CARTESIAN_POINT ( 'NONE',  ( -126.3655805143406354, -25.31862575908220947, 6.461926907689274024 ) ) ;
#45751=EDGE_CURVE ( 'NONE', #8583, #40108, #41505, .T. ) ;
#45752=CARTESIAN_POINT ( 'NONE',  ( -124.5544995689860883, -24.51419770103158768, 9.386484678747164523 ) ) ;
#45753=CARTESIAN_POINT ( 'NONE',  ( -10.60818629614422370, 16.63341085705455669, -1.500000000000002220 ) ) ;
#45754=VERTEX_POINT ( 'NONE', #58236 ) ;
#45756=AXIS2_PLACEMENT_3D ( 'NONE', #61147, #99176, #13446 ) ;
#45763=CARTESIAN_POINT ( 'NONE',  ( -55.62855502628812587, -24.83618233451449697, 1.606449574219536602 ) ) ;
#45764=CARTESIAN_POINT ( 'NONE',  ( -100.2380303841250395, -25.26638540230637631, 7.557070759772178015 ) ) ;
#45766=DIRECTION ( 'NONE',  ( 0.000000000000000000, -2.173523156925979552E-06, 0.9999999999976378895 ) ) ;
#45768=CARTESIAN_POINT ( 'NONE',  ( 18.82558416981596139, 6.732768832687442639, -1.500000000000002220 ) ) ;
#45770=CARTESIAN_POINT ( 'NONE',  ( -72.62287095715005592, -29.50247984919015209, -1.443849546365055359 ) ) ;
#45771=CARTESIAN_POINT ( 'NONE',  ( -45.67376991709483036, -23.48786465467240703, 11.44779295918255002 ) ) ;
#45775=CARTESIAN_POINT ( 'NONE',  ( -119.6256461673538354, -24.15543982623907837, -0.2315651400026546569 ) ) ;
#45776=CARTESIAN_POINT ( 'NONE',  ( -80.64599816240546204, -23.85049219812686161, 10.88485053497527311 ) ) ;
#45777=EDGE_CURVE ( 'NONE', #79765, #3681, #97066, .T. ) ;
#45778=CARTESIAN_POINT ( 'NONE',  ( -51.52287095715006870, -29.50247984919015209, -1.443849546365058689 ) ) ;
#45779=CARTESIAN_POINT ( 'NONE',  ( -61.62287095715004881, -24.66019654487199020, 8.947790411086131712 ) ) ;
#45780=B_SPLINE_CURVE_WITH_KNOTS ( 'NONE', 3,
 ( #81585, #97304, #59245, #12055, #20664, #12560 ),
 .UNSPECIFIED., .F., .F.,
 ( 4, 2, 4 ),
 ( 0.000000000000000000, 0.001380764517853252287, 0.002761529035706504574 ),
 .UNSPECIFIED. ) ;
#45783=CARTESIAN_POINT ( 'NONE',  ( -45.58953762381671027, -25.00182538069144655, 7.747789668545102870 ) ) ;
#45784=CARTESIAN_POINT ( 'NONE',  ( -58.62287095715004881, -24.66019654487199020, 8.947790411086131712 ) ) ;
#45787=EDGE_LOOP ( 'NONE', ( #22233, #4371, #35341, #15838 ) ) ;
#45788=CARTESIAN_POINT ( 'NONE',  ( -14.64122064730360862, 14.02963135428074004, 11.49999999999998934 ) ) ;
#45790=CARTESIAN_POINT ( 'NONE',  ( -61.52287095715007581, -23.47593901973090169, -1.443836447538997092 ) ) ;
#45791=EDGE_CURVE ( 'NONE', #20125, #32109, #88638, .T. ) ;
#45793=CARTESIAN_POINT ( 'NONE',  ( -83.62287095715005592, -23.48783264082478794, -1.443836473390065711 ) ) ;
#45795=CARTESIAN_POINT ( 'NONE',  ( -72.52287095715010423, -24.66019654487199375, 8.947790411086128159 ) ) ;
#45796=CARTESIAN_POINT ( 'NONE',  ( 10.61947033613929214, 17.11087026910869469, -1.500000000000002220 ) ) ;
#45797=CARTESIAN_POINT ( 'NONE',  ( 0.4554788648648982474, -21.05657754196055009, 11.49999999999999645 ) ) ;
#45798=CARTESIAN_POINT ( 'NONE',  ( -127.5228709571500616, -23.48786465467242479, 11.44779295918253581 ) ) ;
#45799=CARTESIAN_POINT ( 'NONE',  ( -18.93877658415168241, -11.43451605920036052, -1.500000000000002220 ) ) ;
#45800=CARTESIAN_POINT ( 'NONE',  ( -0.1859688948871585645, 20.53422428922035081, -1.500000000000002220 ) ) ;
#45805=DIRECTION ( 'NONE',  ( 0.000000000000000000, -2.173523156925980399E-06, 0.9999999999976378895 ) ) ;
#45806=ORIENTED_EDGE ( 'NONE', *, *, #44763, .F. ) ;
#45808=CARTESIAN_POINT ( 'NONE',  ( -29.52287095715006515, -23.38906523657919578, -1.443836447538998424 ) ) ;
#45809=ORIENTED_EDGE ( 'NONE', *, *, #54572, .F. ) ;
#45811=ORIENTED_EDGE ( 'NONE', *, *, #98087, .F. ) ;
#45813=CARTESIAN_POINT ( 'NONE',  ( -74.52287095715004739, -24.66019654487200441, 8.947790411086112172 ) ) ;
#45814=CARTESIAN_POINT ( 'NONE',  ( -68.60862620934042866, -23.48786465467241058, 11.44779295918254824 ) ) ;
#45815=CARTESIAN_POINT ( 'NONE',  ( 6.115004186001010922, -19.73231167505474559, -1.500000000000002220 ) ) ;
#45816=CARTESIAN_POINT ( 'NONE',  ( -13.25059585359799108, -17.08168364658555305, 11.49999999999999645 ) ) ;
#45817=ORIENTED_EDGE ( 'NONE', *, *, #4084, .F. ) ;
#45818=VECTOR ( 'NONE', #35087, 1000.000000000000114 ) ;
#45819=B_SPLINE_CURVE_WITH_KNOTS ( 'NONE', 3,
 ( #29822, #47426, #45066, #742 ),
 .UNSPECIFIED., .F., .F.,
 ( 4, 4 ),
 ( 0.000000000000000000, 9.999999999998897304E-05 ),
 .UNSPECIFIED. ) ;
#45822=CARTESIAN_POINT ( 'NONE',  ( -18.94483701893047467, 11.91932228829616669, -1.500000000000002220 ) ) ;
#45823=FACE_OUTER_BOUND ( 'NONE', #22714, .T. ) ;
#45824=CARTESIAN_POINT ( 'NONE',  ( -67.62287095715005592, -29.50247984919015209, -1.443849546365055359 ) ) ;
#45826=CARTESIAN_POINT ( 'NONE',  ( -99.83329133075007178, -25.30639137160515872, 4.526400298129594546 ) ) ;
#45827=CARTESIAN_POINT ( 'NONE',  ( -49.51415851261705825, -23.73791477778911840, 11.05961554403170943 ) ) ;
#45828=B_SPLINE_CURVE_WITH_KNOTS ( 'NONE', 3,
 ( #28214, #59172, #88623, #67289 ),
 .UNSPECIFIED., .F., .F.,
 ( 4, 4 ),
 ( 0.000000000000000000, 1.000000000000000000 ),
 .UNSPECIFIED. ) ;
#45829=VECTOR ( 'NONE', #39143, 1000.000000000000114 ) ;
#45830=CARTESIAN_POINT ( 'NONE',  ( -33.52287095715006870, -24.50216790748204332, 0.6166512839542452884 ) ) ;
#45831=CARTESIAN_POINT ( 'NONE',  ( -20.86263692406621928, 1.606387762444034362, -1.500000000000002220 ) ) ;
#45832=ORIENTED_EDGE ( 'NONE', *, *, #97660, .F. ) ;
#45833=CARTESIAN_POINT ( 'NONE',  ( -67.60893110983315069, -23.48786465467241058, 11.44779295918254824 ) ) ;
#45834=ORIENTED_EDGE ( 'NONE', *, *, #48399, .T. ) ;
#45835=ORIENTED_EDGE ( 'NONE', *, *, #25362, .T. ) ;
#45837=CARTESIAN_POINT ( 'NONE',  ( -109.5507735056359451, -24.51419770103157347, 9.386484678747171628 ) ) ;
#45838=CARTESIAN_POINT ( 'NONE',  ( 20.79131504077403747, 4.132458064796619368, -1.500000000000002220 ) ) ;
#45839=ORIENTED_EDGE ( 'NONE', *, *, #22030, .T. ) ;
#45840=CARTESIAN_POINT ( 'NONE',  ( -112.5228709571500900, -23.72773821059536914, 11.05748984161097326 ) ) ;
#45841=CARTESIAN_POINT ( 'NONE',  ( -99.47310917600722746, -25.12215581454282542, 6.670037910655527646 ) ) ;
#45842=CARTESIAN_POINT ( 'NONE',  ( 20.57308398666954119, -7.222494929537193187, -1.500000000000002220 ) ) ;
#45843=CARTESIAN_POINT ( 'NONE',  ( -89.06226385320383088, -25.22391154813773895, 6.409327647370975711 ) ) ;
#45844=CARTESIAN_POINT ( 'NONE',  ( -76.64821883033769723, -23.48786465467240703, 11.44779295918254647 ) ) ;
#45845=CARTESIAN_POINT ( 'NONE',  ( -80.33745650938216443, -25.13434931566261099, 7.094763183326051603 ) ) ;
#45846=CARTESIAN_POINT ( 'NONE',  ( 15.22768361601695020, -15.61070304372801587, -1.500000000000002220 ) ) ;
#45847=CARTESIAN_POINT ( 'NONE',  ( -71.70841769935768184, -25.24674343745607885, 6.192981443898670335 ) ) ;
#45852=EDGE_LOOP ( 'NONE', ( #69265, #55702, #74888, #93699 ) ) ;
#45858=CARTESIAN_POINT ( 'NONE',  ( 20.83148622972472808, -3.941400823363257366, -1.500000000000002220 ) ) ;
#45860=CARTESIAN_POINT ( 'NONE',  ( -95.62287095714994223, -24.62285846362214059, 9.038163152653520882 ) ) ;
#45864=VECTOR ( 'NONE', #92182, 1000.000000000000114 ) ;
#45865=CARTESIAN_POINT ( 'NONE',  ( -11.15089393765527959, -15.82809448842462885, -1.500000000000002220 ) ) ;
#45866=CARTESIAN_POINT ( 'NONE',  ( -39.98583224850788298, -25.11539320593059443, 2.804431443241629740 ) ) ;
#45868=CARTESIAN_POINT ( 'NONE',  ( 4.201609111248720829, -18.99613120386805676, 11.49999999999999645 ) ) ;
#45869=DIRECTION ( 'NONE',  ( 0.000000000000000000, 0.9999999999976377785, 2.173523156925979975E-06 ) ) ;
#45872=B_SPLINE_CURVE_WITH_KNOTS ( 'NONE', 3,
 ( #80702, #10695, #11191, #73101 ),
 .UNSPECIFIED., .F., .F.,
 ( 4, 4 ),
 ( 0.000000000000000000, 9.999999999997510880E-05 ),
 .UNSPECIFIED. ) ;
#45873=ORIENTED_EDGE ( 'NONE', *, *, #91905, .F. ) ;
#45875=EDGE_CURVE ( 'NONE', #87834, #86594, #23180, .T. ) ;
#45877=ADVANCED_FACE ( 'NONE', ( #50613 ), #46784, .T. ) ;
#45879=CARTESIAN_POINT ( 'NONE',  ( -93.60100369702254852, -23.48786465467241058, 11.44779295918254469 ) ) ;
#45880=CARTESIAN_POINT ( 'NONE',  ( 18.70796670040472165, 5.986831462552164140, 11.49999999999998934 ) ) ;
#45882=CARTESIAN_POINT ( 'NONE',  ( -41.42418673051398770, -25.27806002644363303, 4.451104005806604036 ) ) ;
#45883=ORIENTED_EDGE ( 'NONE', *, *, #19962, .T. ) ;
#45884=EDGE_CURVE ( 'NONE', #73093, #52694, #31320, .T. ) ;
#45885=CARTESIAN_POINT ( 'NONE',  ( 8.794441374123232791, -19.68457759291379716, -1.500000000000002220 ) ) ;
#45886=CARTESIAN_POINT ( 'NONE',  ( -33.65850923073764989, -23.73791477778911130, 11.05961554403171299 ) ) ;
#45887=CARTESIAN_POINT ( 'NONE',  ( -73.92287095715006728, -23.47593901973090169, -1.443836447538997536 ) ) ;
#45888=CARTESIAN_POINT ( 'NONE',  ( -121.5562042904833788, -24.64898659630529210, 1.056161002820831030 ) ) ;
#45889=CARTESIAN_POINT ( 'NONE',  ( 6.753845092018655016, 22.03294598498517232, -1.500000000000002220 ) ) ;
#45891=CARTESIAN_POINT ( 'NONE',  ( -93.59418303358040703, -23.96119346886880663, -0.6495511937832079141 ) ) ;
#45892=CARTESIAN_POINT ( 'NONE',  ( -51.31007370257843547, -25.18370859199909972, 3.285367768258824483 ) ) ;
#45893=CARTESIAN_POINT ( 'NONE',  ( 12.15850541088210868, 16.18036119754114566, 11.49999999999999645 ) ) ;
#45894=CARTESIAN_POINT ( 'NONE',  ( -121.5213653170695096, -23.73791477778912551, 11.05961554403170055 ) ) ;
#45896=CARTESIAN_POINT ( 'NONE',  ( -111.7814946224345789, -25.10921699980403687, 4.332404819734247958 ) ) ;
#45897=PLANE ( 'NONE',  #76386 ) ;
#45899=CARTESIAN_POINT ( 'NONE',  ( 18.24224480919323810, -7.949361806615760528, 11.49999999999998934 ) ) ;
#45900=EDGE_CURVE ( 'NONE', #96177, #7232, #84608, .T. ) ;
#45903=CARTESIAN_POINT ( 'NONE',  ( -19.76903914530799966, 0.2396048511829373395, -1.500000000000002220 ) ) ;
#45908=CARTESIAN_POINT ( 'NONE',  ( -105.5228709571500616, -24.99132157543084887, 2.256160258750667502 ) ) ;
#45909=CARTESIAN_POINT ( 'NONE',  ( -4.528870947376731237, 20.18191347215651987, 11.49999999999999645 ) ) ;
#45911=EDGE_CURVE ( 'NONE', #16912, #1680, #87469, .T. ) ;
#45912=CARTESIAN_POINT ( 'NONE',  ( -39.52287095715006870, -24.66019654487198665, 8.947790411086131712 ) ) ;
#45913=CARTESIAN_POINT ( 'NONE',  ( -0.6305239314742796530, -22.70799625201654592, 11.49999999999999645 ) ) ;
#45915=CARTESIAN_POINT ( 'NONE',  ( -67.52287095715003318, -23.47593901973090169, -1.443836447538996870 ) ) ;
#45917=CARTESIAN_POINT ( 'NONE',  ( -74.62287095715005592, -23.96177878511307924, 10.65340807706329862 ) ) ;
#45918=CARTESIAN_POINT ( 'NONE',  ( 12.02422309597069017, 16.21794576832014556, 11.49999999999998934 ) ) ;
#45921=CARTESIAN_POINT ( 'NONE',  ( -52.55620429048339304, -23.47593901973091235, -1.443836447539009749 ) ) ;
#45922=ORIENTED_EDGE ( 'NONE', *, *, #11089, .F. ) ;
#45923=EDGE_CURVE ( 'NONE', #12467, #52403, #74182, .T. ) ;
#45924=VERTEX_POINT ( 'NONE', #75982 ) ;
#45925=VECTOR ( 'NONE', #85203, 1000.000000000000227 ) ;
#45926=PLANE ( 'NONE',  #95459 ) ;
#45927=CARTESIAN_POINT ( 'NONE',  ( 19.54225192528841859, -11.95493969655435151, 11.49999999999998934 ) ) ;
#45928=CARTESIAN_POINT ( 'NONE',  ( -50.43601667505130592, -25.18439649994563823, 3.294780684294133177 ) ) ;
#45930=CARTESIAN_POINT ( 'NONE',  ( -3.891998276399621481, 21.28400606017829233, -1.500000000000002220 ) ) ;
#45931=CARTESIAN_POINT ( 'NONE',  ( -123.6266572008115787, -23.48783264082477373, -1.443836473390086361 ) ) ;
#45932=CARTESIAN_POINT ( 'NONE',  ( -34.64253015005402858, -24.15543982623907127, -0.2315651400026574880 ) ) ;
#45933=CARTESIAN_POINT ( 'NONE',  ( 8.468106961216914641, 19.09613275528424836, 11.49999999999999645 ) ) ;
#45934=EDGE_LOOP ( 'NONE', ( #95859, #49082, #36221, #48581 ) ) ;
#45935=CARTESIAN_POINT ( 'NONE',  ( -124.5222546880168437, -23.48783264082477373, -1.443836473390086139 ) ) ;
#45936=CARTESIAN_POINT ( 'NONE',  ( -21.12052157030387889, 6.262089831203976331, 11.49999999999998934 ) ) ;
#45937=CARTESIAN_POINT ( 'NONE',  ( -105.5864560779018433, -24.83644354573579349, 8.397322867130096569 ) ) ;
#45938=CARTESIAN_POINT ( 'NONE',  ( -41.86334916006617135, -25.29087293436575479, 4.024172904988462918 ) ) ;
#45944=DIRECTION ( 'NONE',  ( -3.773278334453079618E-23, 0.9999999999976377785, 2.173523156925978705E-06 ) ) ;
#45945=ORIENTED_EDGE ( 'NONE', *, *, #65753, .F. ) ;
#45946=VECTOR ( 'NONE', #8037, 1000.000000000000114 ) ;
#45948=CARTESIAN_POINT ( 'NONE',  ( -71.53799170295864940, -24.66019654487199730, 8.947790411086113949 ) ) ;
#45949=CARTESIAN_POINT ( 'NONE',  ( -95.62287095715002749, -24.15516710230295416, 10.28746687063724785 ) ) ;
#45951=CARTESIAN_POINT ( 'NONE',  ( -16.48689143942861079, 12.14541645011370541, -1.500000000000002220 ) ) ;
#45956=CARTESIAN_POINT ( 'NONE',  ( 9.404896790668452411, 20.21284700076377305, 11.49999999999998934 ) ) ;
#45958=CARTESIAN_POINT ( 'NONE',  ( -88.62287095715002749, -24.66019654487199730, 8.947790411086128159 ) ) ;
#45961=CARTESIAN_POINT ( 'NONE',  ( -86.62287095715004170, -24.64898659630528854, 1.056161002820827921 ) ) ;
#45962=CARTESIAN_POINT ( 'NONE',  ( 8.324980675869593227, 19.10421180063631752, 11.49999999999998934 ) ) ;
#45963=ORIENTED_EDGE ( 'NONE', *, *, #24913, .F. ) ;
#45965=VERTEX_POINT ( 'NONE', #92708 ) ;
#45966=B_SPLINE_SURFACE_WITH_KNOTS ( 'NONE', 3, 3, ( 
 ( #8688, #95919, #17292, #24899 ),
 ( #95420, #26413, #79689, #40643 ),
 ( #48257, #2584, #55370, #85808 ),
 ( #47755, #79188, #16288, #1075 ),
 ( #33026, #62990, #64002, #33521 ),
 ( #94916, #9177, #1583, #40138 ),
 ( #25407, #56382, #17801, #10186 ) ),
 .UNSPECIFIED., .F., .F., .F.,
 ( 4, 3, 4 ),
 ( 4, 4 ),
 ( 0.7945040050992253633, 0.8970133687736512318, 0.9995227324480769893 ),
 ( 0.9897455052912615958, 0.9912151620501660210 ),
 .UNSPECIFIED. ) ;
#45967=CARTESIAN_POINT ( 'NONE',  ( -51.52589570729855950, -25.25854379533914695, 6.227983929447254319 ) ) ;
#45968=ORIENTED_EDGE ( 'NONE', *, *, #78779, .T. ) ;
#45971=CARTESIAN_POINT ( 'NONE',  ( -121.5562042904833788, -23.48786465467241769, 11.44779295918253759 ) ) ;
#45973=DIRECTION ( 'NONE',  ( -3.773278334453079030E-23, 0.9999999999976377785, 2.173523156925979128E-06 ) ) ;
#45974=DIRECTION ( 'NONE',  ( -3.773278334444166432E-23, 1.000000000000000000, 0.000000000000000000 ) ) ;
#45975=DIRECTION ( 'NONE',  ( 3.773278334444166432E-23, -1.000000000000000000, 0.000000000000000000 ) ) ;
#45976=CARTESIAN_POINT ( 'NONE',  ( 17.03105324785762420, 14.15717209551829647, 11.49999999999999645 ) ) ;
#45977=ORIENTED_EDGE ( 'NONE', *, *, #86529, .T. ) ;
#45980=CARTESIAN_POINT ( 'NONE',  ( 0.4201012023153268271, 22.63755686032812164, 11.49999999999998934 ) ) ;
#45981=CARTESIAN_POINT ( 'NONE',  ( -92.52287095715003318, -24.51283580621460345, 0.6167428607048187628 ) ) ;
#45983=B_SPLINE_CURVE_WITH_KNOTS ( 'NONE', 3,
 ( #61508, #29038, #38145, #45278, #77197, #44780 ),
 .UNSPECIFIED., .F., .F.,
 ( 4, 2, 4 ),
 ( 0.000000000000000000, 0.001380764517853255323, 0.002761529035706510645 ),
 .UNSPECIFIED. ) ;
#45985=EDGE_LOOP ( 'NONE', ( #41682, #86276, #27109, #25714 ) ) ;
#45986=CARTESIAN_POINT ( 'NONE',  ( -99.62287095715005592, -24.65952944569304961, 1.056160979905702124 ) ) ;
#45987=EDGE_CURVE ( 'NONE', #89509, #35626, #85106, .T. ) ;
#45988=CARTESIAN_POINT ( 'NONE',  ( -20.11654390397962544, -0.4351469013266864860, 11.49999999999998934 ) ) ;
#45990=ORIENTED_EDGE ( 'NONE', *, *, #57691, .F. ) ;
#45992=CARTESIAN_POINT ( 'NONE',  ( -4.763361739610138201, -21.85411462188651299, -1.500000000000002220 ) ) ;
#45995=CARTESIAN_POINT ( 'NONE',  ( -101.4413695709857990, -25.16257366102977144, 6.524206556767607523 ) ) ;
#45996=CARTESIAN_POINT ( 'NONE',  ( -81.87214700851818350, -25.22769362155178641, 6.379145389457276494 ) ) ;
#45999=ADVANCED_FACE ( 'NONE', ( #10483 ), #48574, .F. ) ;
#46000=CARTESIAN_POINT ( 'NONE',  ( -68.52287095715004739, -24.51387760970724372, 9.387446482453414731 ) ) ;
#46003=CARTESIAN_POINT ( 'NONE',  ( 15.26536572251939461, -12.21375333317339695, -1.500000000000002220 ) ) ;
#46004=DIRECTION ( 'NONE',  ( 0.000000000000000000, -0.9999999999976377785, -2.173523156925979975E-06 ) ) ;
#46006=CARTESIAN_POINT ( 'NONE',  ( -20.95461191387366284, 4.708766595171775649, -1.500000000000002220 ) ) ;
#46009=CARTESIAN_POINT ( 'NONE',  ( -129.5228709571501042, -23.96177878511308990, 10.65340807706329329 ) ) ;
#46010=CARTESIAN_POINT ( 'NONE',  ( 1.119804705421552748, 22.86502198858056545, -1.500000000000002220 ) ) ;
#46011=VECTOR ( 'NONE', #87692, 1000.000000000000114 ) ;
#46015=CARTESIAN_POINT ( 'NONE',  ( 19.28819943863484454, -5.468471092112969778, 11.49999999999999645 ) ) ;
#46016=CARTESIAN_POINT ( 'NONE',  ( -79.58953762381672448, -23.48783264082478794, -1.443836473390065489 ) ) ;
#46017=DIRECTION ( 'NONE',  ( -3.773278334453079030E-23, 0.9999999999976377785, 2.173523156925979128E-06 ) ) ;
#46020=FACE_OUTER_BOUND ( 'NONE', #94750, .T. ) ;
#46021=VERTEX_POINT ( 'NONE', #48059 ) ;
#46023=ADVANCED_FACE ( 'NONE', ( #87619 ), #39937, .F. ) ;
#46024=CARTESIAN_POINT ( 'NONE',  ( -115.6228709571500559, -23.48786465467242479, 11.44779295918253759 ) ) ;
#46025=CARTESIAN_POINT ( 'NONE',  ( 20.88924836996103451, 6.054424527964996194, 11.49999999999998934 ) ) ;
#46026=CARTESIAN_POINT ( 'NONE',  ( -45.52287095715007581, -24.83620972994591725, 8.398175272781367440 ) ) ;
#46027=CARTESIAN_POINT ( 'NONE',  ( 19.39309126630920588, -2.812899550206792831, -1.500000000000002220 ) ) ;
#46028=CARTESIAN_POINT ( 'NONE',  ( -59.56094173781918499, -29.50249039766296022, 3.409318347773680369 ) ) ;
#46030=CARTESIAN_POINT ( 'NONE',  ( -110.0852742341990904, -25.31698216522971379, 5.455857398936061031 ) ) ;
#46034=CARTESIAN_POINT ( 'NONE',  ( 17.04084431845542369, 11.38269047019995206, 11.49999999999999645 ) ) ;
#46035=CARTESIAN_POINT ( 'NONE',  ( -39.29848179823069643, -25.31692503256359572, 5.130235141806659627 ) ) ;
#46036=EDGE_CURVE ( 'NONE', #84750, #29911, #65648, .T. ) ;
#46040=CARTESIAN_POINT ( 'NONE',  ( -62.52287095715009002, -23.95044443724992078, 10.65354141964649592 ) ) ;
#46042=CARTESIAN_POINT ( 'NONE',  ( -125.5194281211166896, -24.92592662359561828, 8.075495903018000021 ) ) ;
#46044=CARTESIAN_POINT ( 'NONE',  ( -51.93149462243456327, -29.50249640685361641, 6.174041905459458413 ) ) ;
#46045=VECTOR ( 'NONE', #113, 1000.000000000000114 ) ;
#46048=CARTESIAN_POINT ( 'NONE',  ( -21.01138170180016118, -9.542296329091309204, 11.49999999999999645 ) ) ;
#46049=CARTESIAN_POINT ( 'NONE',  ( 22.20067557195093855, 5.203973054738295190, 11.49999999999998934 ) ) ;
#46054=CARTESIAN_POINT ( 'NONE',  ( 22.37589550080693712, 1.095942408959037273, 11.49999999999999645 ) ) ;
#46055=CARTESIAN_POINT ( 'NONE',  ( -74.52287095715004739, -24.66019654487200441, 8.947790411086112172 ) ) ;
#46056=CARTESIAN_POINT ( 'NONE',  ( -47.52287095715006160, -23.48786465467240347, 11.44779295918255002 ) ) ;
#46057=EDGE_CURVE ( 'NONE', #87641, #19622, #60893, .T. ) ;
#46058=CARTESIAN_POINT ( 'NONE',  ( 0.1985894851802381678, 21.93841921393417849, 11.49999999999998934 ) ) ;
#46060=CARTESIAN_POINT ( 'NONE',  ( -87.62875044884228259, -24.35071581493543391, 9.817618358456025263 ) ) ;
#46061=DIRECTION ( 'NONE',  ( 1.000000000000000000, 3.773278334444167608E-23, 8.201307833595939069E-29 ) ) ;
#46062=CARTESIAN_POINT ( 'NONE',  ( -48.90931483959620607, -25.21642463136752710, 6.474588610440971337 ) ) ;
#46064=ORIENTED_EDGE ( 'NONE', *, *, #54936, .F. ) ;
#46065=CARTESIAN_POINT ( 'NONE',  ( -17.80769721941407369, -10.09151516499986734, 11.49999999999998934 ) ) ;
#46066=VERTEX_POINT ( 'NONE', #18102 ) ;
#46067=ORIENTED_EDGE ( 'NONE', *, *, #13678, .T. ) ;
#46070=CARTESIAN_POINT ( 'NONE',  ( 14.79121776280621425, -17.69394282334246427, 11.49999999999998934 ) ) ;
#46073=CARTESIAN_POINT ( 'NONE',  ( -18.19507518397214341, 8.946258903265221107, -1.500000000000002220 ) ) ;
#46074=ORIENTED_EDGE ( 'NONE', *, *, #56955, .T. ) ;
#46075=CARTESIAN_POINT ( 'NONE',  ( -30.30596983276391754, -23.44958398067863925, 11.44779298504228038 ) ) ;
#46076=LINE ( 'NONE', #76995, #20654 ) ;
#46077=CARTESIAN_POINT ( 'NONE',  ( -101.1944152955115186, -25.17323144036708626, 6.858246026757193192 ) ) ;
#46078=PLANE ( 'NONE',  #36673 ) ;
#46079=CARTESIAN_POINT ( 'NONE',  ( -5.333777546869826303, -20.73983961313815172, 11.49999999999999645 ) ) ;
#46080=ORIENTED_EDGE ( 'NONE', *, *, #9119, .F. ) ;
#46083=ORIENTED_EDGE ( 'NONE', *, *, #16259, .F. ) ;
#46084=CARTESIAN_POINT ( 'NONE',  ( -17.53982812869053731, -11.02811673548155902, -1.500000000000002220 ) ) ;
#46087=ORIENTED_EDGE ( 'NONE', *, *, #3031, .F. ) ;
#46089=ORIENTED_EDGE ( 'NONE', *, *, #20566, .T. ) ;
#46090=VERTEX_POINT ( 'NONE', #63806 ) ;
#46092=CARTESIAN_POINT ( 'NONE',  ( -76.52287095715007581, -24.51387760970724372, 9.387446482453411178 ) ) ;
#46093=CARTESIAN_POINT ( 'NONE',  ( -15.43752342082821905, -15.63289427301443801, 11.49999999999999645 ) ) ;
#46094=CARTESIAN_POINT ( 'NONE',  ( -89.52215892217839155, -23.48786465467241413, 11.44779295918254292 ) ) ;
#46095=CARTESIAN_POINT ( 'NONE',  ( -0.2110286175373513040, -22.56517410205234597, 11.49999999999998934 ) ) ;
#46096=CARTESIAN_POINT ( 'NONE',  ( -18.84683179826791743, -9.195131953753229226, 11.49999999999998934 ) ) ;
#46097=CARTESIAN_POINT ( 'NONE',  ( -111.5895376238167245, -24.64898659630368627, 1.056161002820391825 ) ) ;
#46099=ORIENTED_EDGE ( 'NONE', *, *, #65268, .T. ) ;
#46102=CARTESIAN_POINT ( 'NONE',  ( -88.52287095715000476, -23.95044443724992078, 10.65354141964648704 ) ) ;
#46104=CARTESIAN_POINT ( 'NONE',  ( 20.96596170256846747, -4.772324250704091497, -1.500000000000002220 ) ) ;
#46106=ORIENTED_EDGE ( 'NONE', *, *, #38567, .T. ) ;
#46107=CARTESIAN_POINT ( 'NONE',  ( 9.660767377612277329, -18.76748907076374095, -1.500000000000002220 ) ) ;
#46108=PLANE ( 'NONE',  #83823 ) ;
#46109=ADVANCED_FACE ( 'NONE', ( #49067 ), #7059, .T. ) ;
#46110=FACE_OUTER_BOUND ( 'NONE', #35711, .T. ) ;
#46111=CARTESIAN_POINT ( 'NONE',  ( -50.12585357699241939, -25.30188792181875357, 4.702141515391761395 ) ) ;
#46114=CARTESIAN_POINT ( 'NONE',  ( 17.13038851031509680, -14.05419017248541813, -1.500000000000002220 ) ) ;
#46116=CARTESIAN_POINT ( 'NONE',  ( -111.5228709571500190, -23.48783264082477018, -1.443836473390084585 ) ) ;
#46119=ORIENTED_EDGE ( 'NONE', *, *, #79834, .F. ) ;
#46120=CARTESIAN_POINT ( 'NONE',  ( -51.44679290749079570, -25.31633139922050191, 5.195306718205446650 ) ) ;
#46121=CARTESIAN_POINT ( 'NONE',  ( -64.55620429048339304, -23.47593901973091235, -1.443836447539007972 ) ) ;
#46123=ADVANCED_FACE ( 'NONE', ( #4387 ), #51560, .F. ) ;
#46124=CARTESIAN_POINT ( 'NONE',  ( -100.5450588623535282, -24.92564183028979130, 1.928384488918251760 ) ) ;
#46125=CARTESIAN_POINT ( 'NONE',  ( 18.22972481837485859, -6.773019484731225504, -1.500000000000002220 ) ) ;
#46126=CARTESIAN_POINT ( 'NONE',  ( 12.64048258313813733, 17.25876517447949610, 11.49999999999998934 ) ) ;
#46127=CARTESIAN_POINT ( 'NONE',  ( -62.54858697878290741, -24.15543982623907482, -0.2315651400026649265 ) ) ;
#46130=CARTESIAN_POINT ( 'NONE',  ( -37.22287095715007155, -23.47593901973090524, -1.443836447538998424 ) ) ;
#46131=CARTESIAN_POINT ( 'NONE',  ( -11.11902432501355342, 19.77583997595719367, -1.500000000000002220 ) ) ;
#46132=EDGE_CURVE ( 'NONE', #100315, #1307, #51059, .T. ) ;
#46133=CARTESIAN_POINT ( 'NONE',  ( -98.59636335847339694, -23.73766607897669445, -1.055555164236453569 ) ) ;
#46135=CARTESIAN_POINT ( 'NONE',  ( 10.99584971316270732, 16.45119811332560289, 11.49999999999999645 ) ) ;
#46136=CARTESIAN_POINT ( 'NONE',  ( -101.6228709571500559, -24.66019654487199730, 8.947790411086121054 ) ) ;
#46137=B_SPLINE_CURVE_WITH_KNOTS ( 'NONE', 3,
 ( #65332, #41979, #49586, #39959, #72424, #2917 ),
 .UNSPECIFIED., .F., .F.,
 ( 4, 2, 4 ),
 ( 0.000000000000000000, 0.001380901958385396351, 0.002761803916770792702 ),
 .UNSPECIFIED. ) ;
#46140=CARTESIAN_POINT ( 'NONE',  ( -53.62287095715007013, -24.33927499327854704, 9.819080762295818943 ) ) ;
#46141=CARTESIAN_POINT ( 'NONE',  ( -75.52287095715004739, -25.00182538069145366, 7.747789668545101094 ) ) ;
#46142=CARTESIAN_POINT ( 'NONE',  ( 16.85579979752674618, 13.57973486276658903, 11.49999999999998934 ) ) ;
#46144=CARTESIAN_POINT ( 'NONE',  ( 12.26431755764203047, -15.03328313062362298, -1.500000000000002220 ) ) ;
#46145=CARTESIAN_POINT ( 'NONE',  ( -129.6228709571500417, -24.66019654487200086, 8.947790411086117501 ) ) ;
#46146=DIRECTION ( 'NONE',  ( -3.773278334444166432E-23, 1.000000000000000000, 0.000000000000000000 ) ) ;
#46147=CARTESIAN_POINT ( 'NONE',  ( -15.05033210666397103, 12.90603908704162173, 11.49999999999998934 ) ) ;
#46148=ORIENTED_EDGE ( 'NONE', *, *, #69702, .T. ) ;
#46150=CARTESIAN_POINT ( 'NONE',  ( 0.8761431260907562857, 20.31601184897261092, 11.49999999999999645 ) ) ;
#46151=CARTESIAN_POINT ( 'NONE',  ( -80.49978053820711921, -24.63355581998386157, 0.9682620441943954326 ) ) ;
#46154=B_SPLINE_SURFACE_WITH_KNOTS ( 'NONE', 3, 3, ( 
 ( #97729, #14479, #82991, #67801 ),
 ( #68284, #4890, #29218, #35835 ),
 ( #60186, #13980, #91111, #45456 ),
 ( #68780, #83996, #52063, #21587 ),
 ( #44956, #90616, #76370, #53068 ),
 ( #51568, #28724, #6873, #12494 ),
 ( #27726, #67294, #58674, #82009 ) ),
 .UNSPECIFIED., .F., .F., .F.,
 ( 4, 3, 4 ),
 ( 4, 4 ),
 ( 0.0004766839783816705913, 0.1029713700210893035, 0.2054660560637969480 ),
 ( 0.7296796152761164667, 0.7310290126659014787 ),
 .UNSPECIFIED. ) ;
#46155=CARTESIAN_POINT ( 'NONE',  ( -102.5194635214501062, -23.73791477778911840, 11.05961554403170410 ) ) ;
#46156=DIRECTION ( 'NONE',  ( 1.000000000000000000, 3.773278334444167608E-23, 8.201307833595939069E-29 ) ) ;
#46158=CARTESIAN_POINT ( 'NONE',  ( -69.62287095715005592, -29.50247984919015209, -1.443849546365055359 ) ) ;
#46160=CARTESIAN_POINT ( 'NONE',  ( -19.96166555454951208, -2.086822695551191043, -1.500000000000002220 ) ) ;
#46161=CARTESIAN_POINT ( 'NONE',  ( -91.62287095715004170, -29.50250243563736774, 8.947779886222139822 ) ) ;
#46162=ORIENTED_EDGE ( 'NONE', *, *, #16822, .T. ) ;
#46163=CARTESIAN_POINT ( 'NONE',  ( -91.62287095715005592, -24.51387760970725083, 9.387446482453411178 ) ) ;
#46164=CARTESIAN_POINT ( 'NONE',  ( -20.40978113611479827, 10.34812579263477872, 11.49999999999999645 ) ) ;
#46165=CARTESIAN_POINT ( 'NONE',  ( -20.99730734726578874, -8.693733401623333634, 11.49999999999998934 ) ) ;
#46167=CARTESIAN_POINT ( 'NONE',  ( -31.58953762381672092, -23.47596703998600276, 11.44779298504227505 ) ) ;
#46168=CARTESIAN_POINT ( 'NONE',  ( -89.40841769935767047, -25.26877885127129986, 5.947789088311301597 ) ) ;
#46169=CARTESIAN_POINT ( 'NONE',  ( -38.65670220571585247, -23.73791477778911485, 11.05961554403170766 ) ) ;
#46171=ADVANCED_FACE ( 'NONE', ( #89613 ), #43938, .T. ) ;
#46172=CARTESIAN_POINT ( 'NONE',  ( -128.6238584146351798, -24.15620529776629510, 10.23563542870659404 ) ) ;
#46173=CARTESIAN_POINT ( 'NONE',  ( -96.62287095715005592, -29.50250243563736774, 8.947779886222138046 ) ) ;
#46174=VERTEX_POINT ( 'NONE', #65311 ) ;
#46175=CARTESIAN_POINT ( 'NONE',  ( 18.17922461840205983, -9.147185827878928421, 11.49999999999998934 ) ) ;
#46176=ORIENTED_EDGE ( 'NONE', *, *, #63480, .F. ) ;
#46177=CARTESIAN_POINT ( 'NONE',  ( -16.88208375265294237, -15.58181570610299715, -1.500000000000002220 ) ) ;
#46178=CARTESIAN_POINT ( 'NONE',  ( -54.48736948649989387, -24.66019654487199375, 8.947790411086119278 ) ) ;
#46179=VECTOR ( 'NONE', #95258, 1000.000000000000114 ) ;
#46181=CARTESIAN_POINT ( 'NONE',  ( -108.5890470795098821, -24.35071581493544102, 9.817618358456016381 ) ) ;
#46182=CARTESIAN_POINT ( 'NONE',  ( -116.5228709571500474, -24.35013146730204525, 9.818937971375097717 ) ) ;
#46183=CARTESIAN_POINT ( 'NONE',  ( -51.63915185263472551, -24.15620529776628089, 10.23563542870660470 ) ) ;
#46184=CARTESIAN_POINT ( 'NONE',  ( 12.23393567461250697, 17.36540613969008007, 11.49999999999999645 ) ) ;
#46185=EDGE_LOOP ( 'NONE', ( #98203, #44178, #87651, #65839 ) ) ;
#46186=ORIENTED_EDGE ( 'NONE', *, *, #14652, .F. ) ;
#46187=CARTESIAN_POINT ( 'NONE',  ( -0.8134642310582372859, 22.17477653155656725, -1.500000000000002220 ) ) ;
#46188=CARTESIAN_POINT ( 'NONE',  ( -19.88974639711211623, -5.441847772814488948, -1.500000000000002220 ) ) ;
#46190=VERTEX_POINT ( 'NONE', #11984 ) ;
#46191=CARTESIAN_POINT ( 'NONE',  ( -108.9610644980590450, -25.27682616226043777, 4.357072330648456671 ) ) ;
#46193=ORIENTED_EDGE ( 'NONE', *, *, #31712, .F. ) ;
#46194=CARTESIAN_POINT ( 'NONE',  ( -54.52287095715006870, -24.64965694238575011, 8.947790433994203596 ) ) ;
#46195=ORIENTED_EDGE ( 'NONE', *, *, #34820, .F. ) ;
#46197=CARTESIAN_POINT ( 'NONE',  ( -55.62287095715004170, -29.50248789122583659, 2.256150453626215580 ) ) ;
#46198=CARTESIAN_POINT ( 'NONE',  ( 20.50115541507891948, 3.495740877612329101, -1.500000000000002220 ) ) ;
#46199=CARTESIAN_POINT ( 'NONE',  ( -9.430186865587145917, -19.61854929170128869, 11.49999999999999645 ) ) ;
#46200=CARTESIAN_POINT ( 'NONE',  ( -52.62287095715005592, -24.64898659630367561, 1.056161002820821038 ) ) ;
#46201=CARTESIAN_POINT ( 'NONE',  ( -37.62287095715006302, -24.65952944569304250, 1.056160979905693020 ) ) ;
#46202=CARTESIAN_POINT ( 'NONE',  ( -15.54266751046811557, -16.22994250641250957, 11.49999999999998934 ) ) ;
#46203=CARTESIAN_POINT ( 'NONE',  ( -118.5200150627393327, -23.96169478059713853, 10.65365249895717348 ) ) ;
#46206=FACE_OUTER_BOUND ( 'NONE', #37201, .T. ) ;
#46208=B_SPLINE_CURVE_WITH_KNOTS ( 'NONE', 3,
 ( #76427, #52120, #69331, #100251 ),
 .UNSPECIFIED., .F., .F.,
 ( 4, 4 ),
 ( 0.1588721122365702731, 0.1598728592773357438 ),
 .UNSPECIFIED. ) ;
#46210=EDGE_LOOP ( 'NONE', ( #93953, #31168, #16135, #36463 ) ) ;
#46211=ORIENTED_EDGE ( 'NONE', *, *, #4097, .T. ) ;
#46212=ORIENTED_EDGE ( 'NONE', *, *, #18829, .T. ) ;
#46213=CARTESIAN_POINT ( 'NONE',  ( 21.34331307443176584, 0.5271963136488534429, -1.500000000000002220 ) ) ;
#46215=CARTESIAN_POINT ( 'NONE',  ( -17.93810645791062441, 10.97360191750010827, 11.49999999999998934 ) ) ;
#46216=CARTESIAN_POINT ( 'NONE',  ( -30.55801050092156501, -24.27400083755124172, 0.04395666736089842014 ) ) ;
#46218=CARTESIAN_POINT ( 'NONE',  ( -55.55620429048340725, -23.47593901973091235, -1.443836447539007972 ) ) ;
#46219=CARTESIAN_POINT ( 'NONE',  ( -79.11611000704996854, -25.18035200424451858, 3.255061677420811428 ) ) ;
#46220=CARTESIAN_POINT ( 'NONE',  ( 7.969717912702302343, -20.46423023992739942, -1.500000000000002220 ) ) ;
#46221=CARTESIAN_POINT ( 'NONE',  ( -87.52287095715006160, -24.64898659630528854, 1.056161002820827921 ) ) ;
#46222=EDGE_LOOP ( 'NONE', ( #48767, #98058, #26971, #82405 ) ) ;
#46228=EDGE_CURVE ( 'NONE', #14843, #23202, #82000, .T. ) ;
#46230=CARTESIAN_POINT ( 'NONE',  ( -0.1255922731526209202, -21.42410932854645722, 10.97511746239722008 ) ) ;
#46231=CARTESIAN_POINT ( 'NONE',  ( 0.1273799443098547757, 21.28700333820561497, -1.500000000000002220 ) ) ;
#46232=FACE_OUTER_BOUND ( 'NONE', #41358, .T. ) ;
#46233=EDGE_CURVE ( 'NONE', #96245, #79255, #34097, .T. ) ;
#46234=CARTESIAN_POINT ( 'NONE',  ( -52.52287095715006870, -23.47596703998600631, 11.44779298504229104 ) ) ;
#46236=DIRECTION ( 'NONE',  ( 0.7863974287222138537, 0.000000000000000000, 0.6177208787948571533 ) ) ;
#46238=CARTESIAN_POINT ( 'NONE',  ( -11.58057713800463162, -19.31455136971746001, -1.500000000000002220 ) ) ;
#46239=CARTESIAN_POINT ( 'NONE',  ( -111.9729598272094933, -25.06174035403189038, 7.474877196992074424 ) ) ;
#46240=ORIENTED_EDGE ( 'NONE', *, *, #29050, .T. ) ;
#46241=B_SPLINE_CURVE_WITH_KNOTS ( 'NONE', 3,
 ( #36157, #60005, #82814, #66134, #13297, #11813 ),
 .UNSPECIFIED., .F., .F.,
 ( 4, 2, 4 ),
 ( 0.000000000000000000, 0.001380901958385387894, 0.002761803916770775788 ),
 .UNSPECIFIED. ) ;
#46242=CARTESIAN_POINT ( 'NONE',  ( -80.16808653570907950, -25.29573032799826393, 4.512754483485445611 ) ) ;
#46243=CARTESIAN_POINT ( 'NONE',  ( -16.92291128558595048, 9.936001969431544012, 11.49999999999999645 ) ) ;
#46245=CARTESIAN_POINT ( 'NONE',  ( -76.55620429048339304, -24.64965694238574656, 8.947790433994201820 ) ) ;
#46246=EDGE_CURVE ( 'NONE', #28213, #33008, #27220, .T. ) ;
#46247=ORIENTED_EDGE ( 'NONE', *, *, #84335, .F. ) ;
#46250=CARTESIAN_POINT ( 'NONE',  ( -88.50297303682343397, -24.66019654487199730, 8.947790411086115725 ) ) ;
#46251=DIRECTION ( 'NONE',  ( -3.773278334453079618E-23, 0.9999999999976377785, 2.173523156925978705E-06 ) ) ;
#46252=CARTESIAN_POINT ( 'NONE',  ( -91.96401365818223894, -25.31476272485208412, 5.144091107239472827 ) ) ;
#46254=CARTESIAN_POINT ( 'NONE',  ( -14.27994306655487300, -13.59162091658854798, 11.49999999999998934 ) ) ;
#46256=CARTESIAN_POINT ( 'NONE',  ( -109.3584176993576591, -25.28950181196791647, 4.206202504803813191 ) ) ;
#46257=DIRECTION ( 'NONE',  ( -3.773278334453079618E-23, 0.9999999999976377785, 2.173523156925979975E-06 ) ) ;
#46260=CARTESIAN_POINT ( 'NONE',  ( -109.6228709571501128, -24.35013146730204525, 9.818937971375104823 ) ) ;
#46261=CARTESIAN_POINT ( 'NONE',  ( -76.62287095715007013, -24.65952944569304606, 1.056160979905700126 ) ) ;
#46263=DIRECTION ( 'NONE',  ( -3.773278334453079618E-23, 0.9999999999976377785, 2.173523156925979975E-06 ) ) ;
#46266=CARTESIAN_POINT ( 'NONE',  ( -61.52287095715005449, -24.34917612406837151, 0.1852690917426518535 ) ) ;
#46267=CARTESIAN_POINT ( 'NONE',  ( 16.79232260237064978, 10.84791536263152523, -1.500000000000002220 ) ) ;
#46269=CARTESIAN_POINT ( 'NONE',  ( -95.62287095715002749, -25.00182538069145721, 7.747789668545097541 ) ) ;
#46270=CARTESIAN_POINT ( 'NONE',  ( -45.58527553150454992, -24.63419186844611986, 9.035850630976927533 ) ) ;
#46271=VERTEX_POINT ( 'NONE', #41955 ) ;
#46272=EDGE_CURVE ( 'NONE', #95555, #32256, #93386, .T. ) ;
#46273=CARTESIAN_POINT ( 'NONE',  ( -119.5886919143434000, -24.51314013834316086, 0.6176544820404245018 ) ) ;
#46274=VECTOR ( 'NONE', #83338, 1000.000000000000114 ) ;
#46275=CARTESIAN_POINT ( 'NONE',  ( -73.52287095715007581, -23.47596703998600631, 11.44779298504228748 ) ) ;
#46277=CARTESIAN_POINT ( 'NONE',  ( -100.5228709571500616, -25.00182538069145366, 7.747789668545101982 ) ) ;
#46278=PLANE ( 'NONE',  #43201 ) ;
#46279=CARTESIAN_POINT ( 'NONE',  ( -83.52214258138457126, -23.48783264082477018, -1.443836473390093689 ) ) ;
#46281=EDGE_CURVE ( 'NONE', #96695, #73668, #49932, .T. ) ;
#46283=ORIENTED_EDGE ( 'NONE', *, *, #87644, .F. ) ;
#46284=CARTESIAN_POINT ( 'NONE',  ( -20.27173212042777806, -0.06527795377243154895, -1.500000000000002220 ) ) ;
#46285=CARTESIAN_POINT ( 'NONE',  ( -122.5551211338554083, -24.15543982623907482, -0.2315651400026565998 ) ) ;
#46287=FACE_OUTER_BOUND ( 'NONE', #55438, .T. ) ;
#46288=CARTESIAN_POINT ( 'NONE',  ( -90.52287095715006160, -24.99132157543165889, 2.256160258750667502 ) ) ;
#46289=ORIENTED_EDGE ( 'NONE', *, *, #70749, .F. ) ;
#46291=CARTESIAN_POINT ( 'NONE',  ( 19.96388892861992659, -2.714421270036905032, -1.500000000000002220 ) ) ;
#46292=CARTESIAN_POINT ( 'NONE',  ( -20.88184962559319402, -2.832954952542597660, 11.49999999999999645 ) ) ;
#46293=CARTESIAN_POINT ( 'NONE',  ( -13.28819421967561532, -17.68372732473523001, 11.49999999999998934 ) ) ;
#46295=CARTESIAN_POINT ( 'NONE',  ( 17.96566822227200433, 9.963707542159163211, 11.49999999999998934 ) ) ;
#46296=CARTESIAN_POINT ( 'NONE',  ( -95.52214755303867832, -23.48783264082477729, -1.443836473390088804 ) ) ;
#46298=CARTESIAN_POINT ( 'NONE',  ( -53.62287095715004881, -23.48783264082478084, -1.443836473390070596 ) ) ;
#46302=CARTESIAN_POINT ( 'NONE',  ( -64.52287095715006160, -29.50248528299804818, 1.056150453629034924 ) ) ;
#46303=CARTESIAN_POINT ( 'NONE',  ( -85.62287095715002749, -25.00182538069145011, 7.747789668545099317 ) ) ;
#46304=ORIENTED_EDGE ( 'NONE', *, *, #3463, .F. ) ;
#46308=VERTEX_POINT ( 'NONE', #22075 ) ;
#46309=CARTESIAN_POINT ( 'NONE',  ( -36.62287095715005592, -29.50250243563736774, 8.947779886222148704 ) ) ;
#46310=CARTESIAN_POINT ( 'NONE',  ( -50.40895856474225667, -25.03284467579915784, 7.563174216508125269 ) ) ;
#46311=CARTESIAN_POINT ( 'NONE',  ( -77.55620429048339304, -24.65952944569304606, 1.056160979905698794 ) ) ;
#46312=CARTESIAN_POINT ( 'NONE',  ( 18.87225196054570020, 8.368929400942139551, -1.500000000000002220 ) ) ;
#46314=CARTESIAN_POINT ( 'NONE',  ( -17.57154585214776077, 12.61476001598989782, 11.49999999999999645 ) ) ;
#46315=ORIENTED_EDGE ( 'NONE', *, *, #92901, .F. ) ;
#46316=CARTESIAN_POINT ( 'NONE',  ( -100.6228709571500701, -23.47596703998600631, 11.44779298504227860 ) ) ;
#46318=CARTESIAN_POINT ( 'NONE',  ( -3.695635658436464244, 22.08213133993951161, -1.500000000000002220 ) ) ;
#46320=CARTESIAN_POINT ( 'NONE',  ( -79.85862890617264043, -25.12205772052471886, 6.918725823854117607 ) ) ;
#46321=CARTESIAN_POINT ( 'NONE',  ( -53.52287095715008292, -23.47593901973090169, -1.443836447538997092 ) ) ;
#46323=CARTESIAN_POINT ( 'NONE',  ( -58.52287095715006160, -24.65952944569304250, 1.056160979905695463 ) ) ;
#46325=DIRECTION ( 'NONE',  ( -3.773278334453079030E-23, 0.9999999999976377785, 2.173523156925979128E-06 ) ) ;
#46326=CARTESIAN_POINT ( 'NONE',  ( -20.36979505965413395, -4.774807507659313721, 11.49999999999998934 ) ) ;
#46327=ORIENTED_EDGE ( 'NONE', *, *, #14947, .T. ) ;
#46328=CARTESIAN_POINT ( 'NONE',  ( -67.54434724194248929, -24.35071581493543746, 9.817618358456023486 ) ) ;
#46330=CARTESIAN_POINT ( 'NONE',  ( -109.5552926830755069, -23.96169478059713498, 10.65365249895717703 ) ) ;
#46331=CARTESIAN_POINT ( 'NONE',  ( 14.81885032312887240, -15.09863332352077592, -1.500000000000002220 ) ) ;
#46332=ORIENTED_EDGE ( 'NONE', *, *, #84822, .T. ) ;
#46333=CARTESIAN_POINT ( 'NONE',  ( -50.62119766888658035, -23.48783264082476308, -1.443836473390096797 ) ) ;
#46334=PLANE ( 'NONE',  #32002 ) ;
#46335=CARTESIAN_POINT ( 'NONE',  ( 6.392671032147439369, 20.83241601264130693, -1.500000000000002220 ) ) ;
#46336=FACE_OUTER_BOUND ( 'NONE', #78137, .T. ) ;
#46337=CARTESIAN_POINT ( 'NONE',  ( -81.52287095715006160, -24.64898659630367916, 1.056161002820826145 ) ) ;
#46339=CARTESIAN_POINT ( 'NONE',  ( -20.57666286913221754, 7.287794730890116313, -1.500000000000002220 ) ) ;
#46340=CARTESIAN_POINT ( 'NONE',  ( -41.62287095715006302, -24.64898659630367561, 1.056161002820819261 ) ) ;
#46342=ORIENTED_EDGE ( 'NONE', *, *, #75431, .F. ) ;
#46344=CARTESIAN_POINT ( 'NONE',  ( -69.92287095715006728, -23.47596703998600631, 11.44779298504227860 ) ) ;
#46345=CARTESIAN_POINT ( 'NONE',  ( -43.62287095715005592, -23.72747288104442021, -1.053458166803663998 ) ) ;
#46348=VERTEX_POINT ( 'NONE', #60178 ) ;
#46351=CARTESIAN_POINT ( 'NONE',  ( -1.563627757057377110, -21.15500258984412696, -1.500000000000002220 ) ) ;
#46352=CARTESIAN_POINT ( 'NONE',  ( -94.63645698038313014, -23.73766607897670866, -1.055555164236451349 ) ) ;
#46354=CARTESIAN_POINT ( 'NONE',  ( -80.08103705783366877, -25.03138289048727216, 7.514832880348969013 ) ) ;
#46356=CARTESIAN_POINT ( 'NONE',  ( -89.40841769935767047, -29.50248914370730091, 2.832395270851967073 ) ) ;
#46357=CARTESIAN_POINT ( 'NONE',  ( 17.72857150710123619, 7.855407458714720903, -1.500000000000002220 ) ) ;
#46358=FACE_OUTER_BOUND ( 'NONE', #4642, .T. ) ;
#46360=CARTESIAN_POINT ( 'NONE',  ( -16.97169330436246781, 9.548981535075045102, 11.49999999999999645 ) ) ;
#46362=PLANE ( 'NONE',  #72260 ) ;
#46365=CARTESIAN_POINT ( 'NONE',  ( -93.62287095715005592, -23.47593901973091235, -1.443836447539002865 ) ) ;
#46366=PLANE ( 'NONE',  #83642 ) ;
#46368=DIRECTION ( 'NONE',  ( -3.773278334444166432E-23, 1.000000000000000000, 0.000000000000000000 ) ) ;
#46369=CARTESIAN_POINT ( 'NONE',  ( -93.54915263021753447, -24.35071581493543746, 9.817618358456018157 ) ) ;
#46370=CARTESIAN_POINT ( 'NONE',  ( -11.98250242409135780, 15.54504917500377559, -1.500000000000002220 ) ) ;
#46373=CARTESIAN_POINT ( 'NONE',  ( -4.019545577234938882, 21.20919285897865336, -1.500000000000002220 ) ) ;
#46377=CARTESIAN_POINT ( 'NONE',  ( 16.10802587768190008, -16.50329280669357246, -1.500000000000002220 ) ) ;
#46380=CARTESIAN_POINT ( 'NONE',  ( -129.6228709571500417, -29.50250786944525672, 11.44777988621622633 ) ) ;
#46381=FACE_OUTER_BOUND ( 'NONE', #34593, .T. ) ;
#46382=CARTESIAN_POINT ( 'NONE',  ( -121.5894494653266662, -24.35071581493543391, 9.817618358456025263 ) ) ;
#46383=CARTESIAN_POINT ( 'NONE',  ( -104.5228709571501042, -23.72773821059536914, 11.05748984161097326 ) ) ;
#46386=CARTESIAN_POINT ( 'NONE',  ( -109.4090396635228188, -25.25571914749011881, 3.901050301940306664 ) ) ;
#46387=CARTESIAN_POINT ( 'NONE',  ( -129.5896348228089323, -24.51314013834316796, 0.6176544820404222813 ) ) ;
#46388=CARTESIAN_POINT ( 'NONE',  ( -114.5882167185886260, -24.51419770103159124, 9.386484678747160970 ) ) ;
#46389=CARTESIAN_POINT ( 'NONE',  ( 3.219775368129482285, -19.64489633315863770, -1.500000000000002220 ) ) ;
#46391=CARTESIAN_POINT ( 'NONE',  ( -41.58953762381673158, -23.48783264082477729, -1.443836473390071928 ) ) ;
#46392=CARTESIAN_POINT ( 'NONE',  ( 18.55763160240848109, 7.024834138330111166, -1.500000000000002220 ) ) ;
#46393=VECTOR ( 'NONE', #26582, 1000.000000000000114 ) ;
#46394=CARTESIAN_POINT ( 'NONE',  ( -56.53342923132996845, -24.65952944569304250, 1.056160979905696795 ) ) ;
#46395=ADVANCED_FACE ( 'NONE', ( #13971 ), #61176, .T. ) ;
#46396=CARTESIAN_POINT ( 'NONE',  ( -39.04530173637052570, -25.10925879726424625, 4.154357150429498269 ) ) ;
#46397=DIRECTION ( 'NONE',  ( -0.000000000000000000, 2.173523156925979552E-06, -0.9999999999976378895 ) ) ;
#46398=CARTESIAN_POINT ( 'NONE',  ( -16.63904852704994042, -12.34428335884295969, 11.49999999999999645 ) ) ;
#46399=LINE ( 'NONE', #16944, #58081 ) ;
#46400=CARTESIAN_POINT ( 'NONE',  ( -50.05581273115511465, -25.31439285659850214, 5.236521717157118339 ) ) ;
#46401=CARTESIAN_POINT ( 'NONE',  ( -20.46125754976198508, 9.905080999540670561, 11.49999999999999645 ) ) ;
#46402=ADVANCED_FACE ( 'NONE', ( #29705 ), #6371, .F. ) ;
#46404=DIRECTION ( 'NONE',  ( 1.000000000000000000, 3.773278334444166432E-23, 8.201307841325785021E-29 ) ) ;
#46407=CARTESIAN_POINT ( 'NONE',  ( 19.60372117168125072, 4.849774137724135237, -1.500000000000002220 ) ) ;
#46408=PLANE ( 'NONE',  #9520 ) ;
#46409=CARTESIAN_POINT ( 'NONE',  ( -57.62287095715004881, -29.50250786944525672, 11.44777988621623876 ) ) ;
#46410=VECTOR ( 'NONE', #68304, 1000.000000000000114 ) ;
#46411=ORIENTED_EDGE ( 'NONE', *, *, #49791, .F. ) ;
#46413=CARTESIAN_POINT ( 'NONE',  ( -80.35919894935767616, -29.50249278017872712, 4.505472193924938473 ) ) ;
#46414=CARTESIAN_POINT ( 'NONE',  ( -2.380104427745746154, 22.76713797270899065, -1.500000000000002220 ) ) ;
#46415=CARTESIAN_POINT ( 'NONE',  ( -29.52491602809394422, -24.57633962600280597, 1.056161296257513094 ) ) ;
#46416=CARTESIAN_POINT ( 'NONE',  ( -5.517532219241116032, 20.92096086382833064, -1.500000000000002220 ) ) ;
#46418=CARTESIAN_POINT ( 'NONE',  ( -114.6228709571500133, -24.33832256527049154, 0.1851278514138625098 ) ) ;
#46419=CARTESIAN_POINT ( 'NONE',  ( -17.98194200498208062, 10.70670730041394947, 11.49999999999999645 ) ) ;
#46421=CARTESIAN_POINT ( 'NONE',  ( -69.32616065491644974, -25.24754329150182741, 5.234946919193567361 ) ) ;
#46422=CARTESIAN_POINT ( 'NONE',  ( -16.14483305390557888, 14.99321182834783528, 11.49999999999998934 ) ) ;
#46424=FACE_OUTER_BOUND ( 'NONE', #77846, .T. ) ;
#46425=CARTESIAN_POINT ( 'NONE',  ( -66.52287095715006160, -24.64965694238407323, 8.947790433994200043 ) ) ;
#46427=CARTESIAN_POINT ( 'NONE',  ( -72.62287095715005592, -29.50250243563736774, 8.947779886222143375 ) ) ;
#46429=ORIENTED_EDGE ( 'NONE', *, *, #57111, .T. ) ;
#46430=CARTESIAN_POINT ( 'NONE',  ( -72.54527135507231606, -24.35071581493542681, 9.817618358456032368 ) ) ;
#46431=B_SPLINE_CURVE_WITH_KNOTS ( 'NONE', 3,
 ( #99403, #98397, #52742, #83681 ),
 .UNSPECIFIED., .F., .F.,
 ( 4, 4 ),
 ( 2.775557561562891351E-17, 9.999999999996123101E-05 ),
 .UNSPECIFIED. ) ;
#46433=ORIENTED_EDGE ( 'NONE', *, *, #39416, .F. ) ;
#46434=CARTESIAN_POINT ( 'NONE',  ( -71.64477584057199522, -23.73791477778911840, 11.05961554403170766 ) ) ;
#46435=CARTESIAN_POINT ( 'NONE',  ( -95.62287095715005592, -24.83620972994591725, 8.398175272781362111 ) ) ;
#46437=CARTESIAN_POINT ( 'NONE',  ( -13.28352777634190396, 15.58691228024164310, -1.500000000000002220 ) ) ;
#46438=VERTEX_POINT ( 'NONE', #37331 ) ;
#46439=DIRECTION ( 'NONE',  ( 0.000000000000000000, 2.173523156925980399E-06, -0.9999999999976378895 ) ) ;
#46443=CARTESIAN_POINT ( 'NONE',  ( -22.27612280437926273, 0.2766752662994830247, -1.500000000000002220 ) ) ;
#46447=FACE_OUTER_BOUND ( 'NONE', #37445, .T. ) ;
#46448=EDGE_LOOP ( 'NONE', ( #48733, #66559, #77875, #99716 ) ) ;
#46449=CARTESIAN_POINT ( 'NONE',  ( -73.52287095715007581, -29.50250243563736774, 8.947779886222143375 ) ) ;
#46450=CARTESIAN_POINT ( 'NONE',  ( -28.54076794517382965, -24.63646022460865836, 8.057462240486939820 ) ) ;
#46451=CARTESIAN_POINT ( 'NONE',  ( -15.88994834598175387, -13.44966708658631838, 11.49999999999998934 ) ) ;
#46452=ORIENTED_EDGE ( 'NONE', *, *, #55274, .T. ) ;
#46454=VERTEX_POINT ( 'NONE', #2266 ) ;
#46456=CARTESIAN_POINT ( 'NONE',  ( -50.99155954085787812, -25.25854544672502655, 6.987757701561226220 ) ) ;
#46457=ORIENTED_EDGE ( 'NONE', *, *, #17013, .T. ) ;
#46460=CARTESIAN_POINT ( 'NONE',  ( -55.62287095715004170, -24.91570333823098693, 8.075032458375554612 ) ) ;
#46462=VECTOR ( 'NONE', #81038, 1000.000000000000114 ) ;
#46463=CARTESIAN_POINT ( 'NONE',  ( -51.55620429048339304, -24.65952944569304606, 1.056160979905694131 ) ) ;
#46464=CARTESIAN_POINT ( 'NONE',  ( -92.56173786369195966, -23.48786465467241413, 11.44779295918254469 ) ) ;
#46466=EDGE_CURVE ( 'NONE', #17101, #21, #84942, .T. ) ;
#46467=CARTESIAN_POINT ( 'NONE',  ( -10.71655374829924767, -19.46388382022006525, 11.49999999999999645 ) ) ;
#46468=EDGE_LOOP ( 'NONE', ( #53040, #29381, #92358, #29712 ) ) ;
#46469=CARTESIAN_POINT ( 'NONE',  ( -38.62287095715005592, -23.48783264082477373, -1.443836473390072594 ) ) ;
#46471=CARTESIAN_POINT ( 'NONE',  ( 13.37577147909557773, 18.27418014603220442, 11.49999999999998934 ) ) ;
#46472=AXIS2_PLACEMENT_3D ( 'NONE', #15068, #44026, #36912 ) ;
#46474=ORIENTED_EDGE ( 'NONE', *, *, #31267, .T. ) ;
#46475=VERTEX_POINT ( 'NONE', #86980 ) ;
#46478=CARTESIAN_POINT ( 'NONE',  ( -20.09103079077430820, 1.113595961413322177, -1.500000000000002220 ) ) ;
#46479=ADVANCED_FACE ( 'NONE', ( #64684 ), #94091, .F. ) ;
#46481=EDGE_LOOP ( 'NONE', ( #98136, #93764, #56821, #52452 ) ) ;
#46482=CARTESIAN_POINT ( 'NONE',  ( -42.62287095715004881, -24.66019654487199020, 8.947790411086135265 ) ) ;
#46483=CARTESIAN_POINT ( 'NONE',  ( -6.430504157862594994, -21.42354456762059201, -1.500000000000002220 ) ) ;
#46487=CARTESIAN_POINT ( 'NONE',  ( -101.4810573493621177, -25.25341147194796676, 6.435288862326006054 ) ) ;
#46488=CARTESIAN_POINT ( 'NONE',  ( -119.6228709571500559, -23.95044443724992433, 10.65354141964649592 ) ) ;
#46489=DIRECTION ( 'NONE',  ( 1.000000000000000000, 3.773278334444166432E-23, 8.201307841325785021E-29 ) ) ;
#46490=VECTOR ( 'NONE', #50570, 1000.000000000000114 ) ;
#46494=CARTESIAN_POINT ( 'NONE',  ( 6.866622826037362515, -18.30913693658520103, -1.500000000000002220 ) ) ;
#46495=CARTESIAN_POINT ( 'NONE',  ( -111.6228709571500559, -29.50250243563736774, 8.947779886222136270 ) ) ;
#46496=CARTESIAN_POINT ( 'NONE',  ( 21.22668844964908885, 3.412186807495566132, 11.49999999999998934 ) ) ;
#46498=CARTESIAN_POINT ( 'NONE',  ( -128.5220661547153043, -23.73766607897671932, -1.055555164236423149 ) ) ;
#46500=CARTESIAN_POINT ( 'NONE',  ( -71.52287095715007581, -23.48786465467241058, 11.44779295918254647 ) ) ;
#46501=CARTESIAN_POINT ( 'NONE',  ( -107.6228709571500701, -23.47596703998600631, 11.44779298504227860 ) ) ;
#46502=CARTESIAN_POINT ( 'NONE',  ( 12.51456667378993259, 19.11410217522374921, -1.500000000000002220 ) ) ;
#46504=CARTESIAN_POINT ( 'NONE',  ( -85.62287095715005592, -23.48786465467241413, 11.44779295918254114 ) ) ;
#46505=FACE_OUTER_BOUND ( 'NONE', #54269, .T. ) ;
#46506=CARTESIAN_POINT ( 'NONE',  ( 20.03642891561555928, 0.6179553080306146029, 11.49999999999999645 ) ) ;
#46507=CARTESIAN_POINT ( 'NONE',  ( -79.52287095715004739, -23.48783264082476663, -1.443836473390090358 ) ) ;
#46511=ORIENTED_EDGE ( 'NONE', *, *, #58263, .T. ) ;
#46513=CARTESIAN_POINT ( 'NONE',  ( -109.2319509041356582, -25.19177197432999904, 3.341196461261103590 ) ) ;
#46514=CARTESIAN_POINT ( 'NONE',  ( -15.31764660673900558, 15.41647822393392175, -1.500000000000002220 ) ) ;
#46515=LINE ( 'NONE', #69857, #91695 ) ;
#46516=CARTESIAN_POINT ( 'NONE',  ( 18.62133539762988121, 6.091496293051981148, -1.500000000000002220 ) ) ;
#46517=VECTOR ( 'NONE', #28267, 1000.000000000000114 ) ;
#46518=CARTESIAN_POINT ( 'NONE',  ( -85.52287095715003318, -25.00182538069145011, 7.747789668545101094 ) ) ;
#46520=CARTESIAN_POINT ( 'NONE',  ( -109.9698394925872549, -25.31698189487863715, 5.331473593049757653 ) ) ;
#46522=CARTESIAN_POINT ( 'NONE',  ( -91.62578307729398830, -24.51419770103159124, 9.386484678747176957 ) ) ;
#46524=CARTESIAN_POINT ( 'NONE',  ( 4.502618398017903090, 20.03723546437915104, 11.49999999999999645 ) ) ;
#46525=LINE ( 'NONE', #45535, #84591 ) ;
#46527=CARTESIAN_POINT ( 'NONE',  ( -120.5539087145323833, -24.52300882791530512, 0.6510814631126412566 ) ) ;
#46528=ORIENTED_EDGE ( 'NONE', *, *, #23633, .F. ) ;
#46530=CARTESIAN_POINT ( 'NONE',  ( -100.6814946224345846, -25.31296450754352279, 4.736250530731430430 ) ) ;
#46531=CARTESIAN_POINT ( 'NONE',  ( -39.81688933929658702, -25.28892465615578544, 3.494185961199250290 ) ) ;
#46538=CARTESIAN_POINT ( 'NONE',  ( -124.6228709571501128, -23.96177878511308634, 10.65340807706329507 ) ) ;
#46539=CARTESIAN_POINT ( 'NONE',  ( 18.33865528945960577, 14.04639130150205872, 11.49999999999999645 ) ) ;
#46540=CARTESIAN_POINT ( 'NONE',  ( -18.69919181139871966, -13.08804974640095686, 11.49999999999998934 ) ) ;
#46542=CARTESIAN_POINT ( 'NONE',  ( -75.52287095715013265, -24.14406661686762945, 10.28769366194083901 ) ) ;
#46543=CARTESIAN_POINT ( 'NONE',  ( -123.5228709571501042, -23.48783264082477018, -1.443836473390084141 ) ) ;
#46544=CARTESIAN_POINT ( 'NONE',  ( -21.67104271438225638, 5.786422744429515319, 11.49999999999999645 ) ) ;
#46546=CARTESIAN_POINT ( 'NONE',  ( -106.5562042904834215, -24.64898659630529210, 1.056161002820828587 ) ) ;
#46547=DIRECTION ( 'NONE',  ( 0.000000000000000000, -2.173523156925979552E-06, 0.9999999999976378895 ) ) ;
#46548=CARTESIAN_POINT ( 'NONE',  ( -19.33260374144687077, -10.33727041909969380, 11.49999999999998934 ) ) ;
#46549=B_SPLINE_CURVE_WITH_KNOTS ( 'NONE', 3,
 ( #2940, #10531, #95770, #26261 ),
 .UNSPECIFIED., .F., .F.,
 ( 4, 4 ),
 ( 0.000000000000000000, 1.000000000000000000 ),
 .UNSPECIFIED. ) ;
#46552=CARTESIAN_POINT ( 'NONE',  ( -72.52287095715007581, -29.50248528299804818, 1.056150453629036701 ) ) ;
#46554=CARTESIAN_POINT ( 'NONE',  ( -49.02504946315652035, -25.17378427848792910, 6.789324151856864553 ) ) ;
#46557=CARTESIAN_POINT ( 'NONE',  ( 10.21088607376515789, 17.76353854702842483, -1.500000000000002220 ) ) ;
#46558=ORIENTED_EDGE ( 'NONE', *, *, #9579, .F. ) ;
#46561=ORIENTED_EDGE ( 'NONE', *, *, #13538, .F. ) ;
#46562=CARTESIAN_POINT ( 'NONE',  ( -14.75821945985506645, 17.75411527500383002, -1.500000000000002220 ) ) ;
#46563=CARTESIAN_POINT ( 'NONE',  ( -82.52287095715006160, -23.94994826722564696, -0.6494450866342720285 ) ) ;
#46564=CARTESIAN_POINT ( 'NONE',  ( 0.7435384974594729801, 20.27106041150680937, -1.500000000000002220 ) ) ;
#46566=ADVANCED_FACE ( 'NONE', ( #95101 ), #41734, .T. ) ;
#46568=CARTESIAN_POINT ( 'NONE',  ( -48.52287095715006870, -23.72773821059535848, 11.05748984161097326 ) ) ;
#46570=CARTESIAN_POINT ( 'NONE',  ( -92.56173453440464982, -23.48783264082477729, -1.443836473390063713 ) ) ;
#46572=DIRECTION ( 'NONE',  ( 0.000000000000000000, -0.9999999999976377785, -2.173523156925979975E-06 ) ) ;
#46573=CARTESIAN_POINT ( 'NONE',  ( -70.58187943343651227, -24.83618233451450052, 1.606449574219541487 ) ) ;
#46574=CARTESIAN_POINT ( 'NONE',  ( 8.645823604709390153, 19.67543227842514852, 11.49999999999999645 ) ) ;
#46579=ORIENTED_EDGE ( 'NONE', *, *, #84311, .F. ) ;
#46580=VECTOR ( 'NONE', #8809, 1000.000000000000114 ) ;
#46581=CARTESIAN_POINT ( 'NONE',  ( 6.562613027033147084, 19.67253995144353240, -1.500000000000002220 ) ) ;
#46583=B_SPLINE_CURVE_WITH_KNOTS ( 'NONE', 3,
 ( #14084, #83094, #52663, #91707, #91215, #68882, #22189, #14587 ),
 .UNSPECIFIED., .F., .F.,
 ( 4, 2, 2, 4 ),
 ( -0.001224873891641433234, -0.0002244903592271136998, 0.0007758931731872054007, 0.002776660238015844252 ),
 .UNSPECIFIED. ) ;
#46586=B_SPLINE_SURFACE_WITH_KNOTS ( 'NONE', 3, 3, ( 
 ( #98359, #21729, #43099, #29355 ),
 ( #83133, #28864, #74042, #90261 ),
 ( #74534, #52702, #21234, #35486 ),
 ( #83640, #89766, #5025, #37476 ),
 ( #91747, #76021, #68426, #35973 ),
 ( #20737, #52205, #60828, #59318 ),
 ( #99361, #66943, #44091, #67434 ) ),
 .UNSPECIFIED., .F., .F., .F.,
 ( 4, 3, 4 ),
 ( 4, 4 ),
 ( 0.7945040050992241421, 0.8970133687736505657, 0.9995227324480768782 ),
 ( 0.9297302545846050092, 0.9311722043212208311 ),
 .UNSPECIFIED. ) ;
#46587=CARTESIAN_POINT ( 'NONE',  ( -111.5501932863792973, -24.66019654487200441, 8.947790411086105067 ) ) ;
#46588=LINE ( 'NONE', #63329, #38901 ) ;
#46589=VERTEX_POINT ( 'NONE', #3765 ) ;
#46590=ORIENTED_EDGE ( 'NONE', *, *, #34917, .T. ) ;
#46592=FACE_OUTER_BOUND ( 'NONE', #4142, .T. ) ;
#46593=CARTESIAN_POINT ( 'NONE',  ( -65.49893136555071749, -24.40034930558991277, 0.3402023900116039612 ) ) ;
#46594=EDGE_CURVE ( 'NONE', #67442, #40077, #47395, .T. ) ;
#46595=CARTESIAN_POINT ( 'NONE',  ( -2.093881351098874521, -21.91542971883435698, 11.49999999999999645 ) ) ;
#46596=CARTESIAN_POINT ( 'NONE',  ( -39.04303308397305727, -25.28006866179717349, 4.215216948383927686 ) ) ;
#46597=CARTESIAN_POINT ( 'NONE',  ( -5.352388609804938469, -21.92410630658433845, 11.49999999999998934 ) ) ;
#46599=CARTESIAN_POINT ( 'NONE',  ( 20.99820426035194032, -0.1900765340283884497, -1.500000000000002220 ) ) ;
#46601=B_SPLINE_CURVE_WITH_KNOTS ( 'NONE', 3,
 ( #702, #31649, #62618, #39759 ),
 .UNSPECIFIED., .F., .F.,
 ( 4, 4 ),
 ( 0.000000000000000000, 1.000000000000000000 ),
 .UNSPECIFIED. ) ;
#46603=ORIENTED_EDGE ( 'NONE', *, *, #12125, .F. ) ;
#46606=CARTESIAN_POINT ( 'NONE',  ( -59.62287095715007013, -23.95044443724992433, 10.65354141964650125 ) ) ;
#46607=ADVANCED_FACE ( 'NONE', ( #12845 ), #89984, .F. ) ;
#46609=CARTESIAN_POINT ( 'NONE',  ( -11.62584540149672385, -18.10649092712023389, -1.500000000000002220 ) ) ;
#46610=CARTESIAN_POINT ( 'NONE',  ( -114.6228709571500559, -23.47593901973091235, -1.443836447538999312 ) ) ;
#46612=CARTESIAN_POINT ( 'NONE',  ( 14.81885032312887240, -15.09863332352077592, -1.500000000000002220 ) ) ;
#46613=CARTESIAN_POINT ( 'NONE',  ( -126.6228709571501128, -23.73907113216991860, -1.053371485793222373 ) ) ;
#46614=CARTESIAN_POINT ( 'NONE',  ( -60.72593597384194908, -25.31249728293746770, 5.276660823416809087 ) ) ;
#46615=CARTESIAN_POINT ( 'NONE',  ( -121.5550122312708652, -24.15543982623907127, -0.2315651400026573492 ) ) ;
#46616=AXIS2_PLACEMENT_3D ( 'NONE', #72091, #10678, #9676 ) ;
#46617=CARTESIAN_POINT ( 'NONE',  ( -109.6228709571500559, -24.66019654487199730, 8.947790411086124607 ) ) ;
#46618=CARTESIAN_POINT ( 'NONE',  ( -81.22287095715009286, -23.47593901973090169, -1.443836447538997092 ) ) ;
#46619=CARTESIAN_POINT ( 'NONE',  ( 7.527104757430762128, -20.84474501729809859, -1.500000000000002220 ) ) ;
#46620=CARTESIAN_POINT ( 'NONE',  ( -71.49854048978230026, -24.51314013834315730, 0.6176544820404130665 ) ) ;
#46621=EDGE_CURVE ( 'NONE', #78091, #90318, #70397, .T. ) ;
#46625=CARTESIAN_POINT ( 'NONE',  ( -40.01839366089613748, -25.30501058306510487, 5.509688048021296858 ) ) ;
#46626=ADVANCED_FACE ( 'NONE', ( #49948 ), #27595, .F. ) ;
#46627=PLANE ( 'NONE',  #62547 ) ;
#46628=CARTESIAN_POINT ( 'NONE',  ( -39.55620429048340725, -24.64965694238574656, 8.947790433994205372 ) ) ;
#46629=ADVANCED_FACE ( 'NONE', ( #65183 ), #72777, .T. ) ;
#46630=CARTESIAN_POINT ( 'NONE',  ( 13.32768686175602646, -14.16729652289716057, -1.500000000000002220 ) ) ;
#46631=CARTESIAN_POINT ( 'NONE',  ( 2.027878592902508270, 21.29203748114955985, 11.49999999999998934 ) ) ;
#46632=CARTESIAN_POINT ( 'NONE',  ( -62.62365711165048054, -24.65952944569303895, 1.056160979905693686 ) ) ;
#46633=CARTESIAN_POINT ( 'NONE',  ( -94.62287095715005592, -24.65952944569304606, 1.056160979905700348 ) ) ;
#46634=CARTESIAN_POINT ( 'NONE',  ( -72.52287095715010423, -23.95044443724992789, 10.65354141964649592 ) ) ;
#46635=CARTESIAN_POINT ( 'NONE',  ( -101.0947412695425385, -25.18440065684229623, 3.544729342112358683 ) ) ;
#46636=CARTESIAN_POINT ( 'NONE',  ( -6.316168294299441932, 21.79233575779346310, -1.500000000000002220 ) ) ;
#46638=CARTESIAN_POINT ( 'NONE',  ( -103.6228709571500275, -24.51283580621364067, 0.6167428607019885822 ) ) ;
#46640=CARTESIAN_POINT ( 'NONE',  ( 7.211006999188390942, 18.53272205163514030, 11.49999999999999645 ) ) ;
#46641=CARTESIAN_POINT ( 'NONE',  ( -123.6243254326775087, -24.35071581493544812, 9.817618358456018157 ) ) ;
#46642=CARTESIAN_POINT ( 'NONE',  ( -51.52287095715006870, -24.64965694238407323, 8.947790433994203596 ) ) ;
#46644=CARTESIAN_POINT ( 'NONE',  ( -119.5228709571500758, -29.50247984919015209, -1.443849546365046699 ) ) ;
#46646=CARTESIAN_POINT ( 'NONE',  ( -87.58953762381671027, -23.47596703998600631, 11.44779298504227683 ) ) ;
#46647=CARTESIAN_POINT ( 'NONE',  ( 21.13687465659472409, 4.681744431724916389, 11.49999999999998934 ) ) ;
#46649=CARTESIAN_POINT ( 'NONE',  ( -124.5562042904833646, -24.64898659630529565, 1.056161002820835026 ) ) ;
#46650=CARTESIAN_POINT ( 'NONE',  ( 13.32768686175602646, -14.16729652289716057, -1.500000000000002220 ) ) ;
#46651=CARTESIAN_POINT ( 'NONE',  ( -114.5895376238167103, -24.64965694238407679, 8.947790433994649462 ) ) ;
#46652=CARTESIAN_POINT ( 'NONE',  ( -61.62287095715004881, -23.47596703998600631, 11.44779298504227505 ) ) ;
#46653=CARTESIAN_POINT ( 'NONE',  ( -11.71124675921804403, 15.99993322257668282, 11.49999999999998934 ) ) ;
#46655=CARTESIAN_POINT ( 'NONE',  ( -18.82316870354832616, 7.800066519331792847, 11.49999999999999645 ) ) ;
#46656=CARTESIAN_POINT ( 'NONE',  ( -80.55274853021465731, -24.15503026093913164, -0.2815557561904567518 ) ) ;
#46658=VERTEX_POINT ( 'NONE', #34212 ) ;
#46659=DIRECTION ( 'NONE',  ( -3.773278334453079618E-23, 0.9999999999976377785, 2.173523156925979975E-06 ) ) ;
#46661=CARTESIAN_POINT ( 'NONE',  ( -49.70686029532972583, -25.25214431742755394, 4.960084010147586930 ) ) ;
#46662=CARTESIAN_POINT ( 'NONE',  ( -128.6228709571500417, -23.48783264082479505, -1.443836473390056829 ) ) ;
#46664=CARTESIAN_POINT ( 'NONE',  ( 5.780499401231428358, -19.25771307485560158, -1.500000000000002220 ) ) ;
#46667=CARTESIAN_POINT ( 'NONE',  ( -91.62287095715009855, -23.73934037231758154, 11.05740245334328442 ) ) ;
#46669=CARTESIAN_POINT ( 'NONE',  ( 15.42672287639063100, 16.92133821996916865, 11.49999999999999645 ) ) ;
#46670=CARTESIAN_POINT ( 'NONE',  ( -4.086358941109507370, -22.34742993483353146, -1.500000000000002220 ) ) ;
#46673=CARTESIAN_POINT ( 'NONE',  ( -51.52287095715006870, -23.47596703998600631, 11.44779298504229104 ) ) ;
#46674=CARTESIAN_POINT ( 'NONE',  ( -40.45829750704997707, -25.19502912051678223, 3.293943094755625633 ) ) ;
#46677=CARTESIAN_POINT ( 'NONE',  ( -128.6240059821712975, -23.96169478059714919, 10.65365249895716993 ) ) ;
#46678=CARTESIAN_POINT ( 'NONE',  ( -62.62287095715004881, -29.50248528299804818, 1.056150453629034924 ) ) ;
#46681=AXIS2_PLACEMENT_3D ( 'NONE', #4573, #66493, #58363 ) ;
#46682=CARTESIAN_POINT ( 'NONE',  ( -0.5597704280004801580, 20.37679164443051505, -1.500000000000002220 ) ) ;
#46683=ORIENTED_EDGE ( 'NONE', *, *, #47945, .F. ) ;
#46685=CARTESIAN_POINT ( 'NONE',  ( -22.77861398648627400, -3.026084143414268013, -1.500000000000002220 ) ) ;
#46686=CARTESIAN_POINT ( 'NONE',  ( -45.52287095715006870, -23.84047902841602706, -0.8780736468305712084 ) ) ;
#46687=ADVANCED_FACE ( 'NONE', ( #35207 ), #82858, .T. ) ;
#46688=VERTEX_POINT ( 'NONE', #52426 ) ;
#46689=CARTESIAN_POINT ( 'NONE',  ( -108.5121515958373095, -24.66019654487200086, 8.947790411086106843 ) ) ;
#46692=EDGE_CURVE ( 'NONE', #25473, #294, #36695, .T. ) ;
#46693=CARTESIAN_POINT ( 'NONE',  ( -111.5228709571500758, -24.50321055353805377, 9.387540953477511607 ) ) ;
#46694=CARTESIAN_POINT ( 'NONE',  ( 13.79380260783658407, 16.28676726024703214, 11.49999999999999645 ) ) ;
#46695=ORIENTED_EDGE ( 'NONE', *, *, #88714, .F. ) ;
#46697=CARTESIAN_POINT ( 'NONE',  ( 13.49617185221842952, 17.62045156095830123, -1.500000000000002220 ) ) ;
#46698=CARTESIAN_POINT ( 'NONE',  ( 15.34805171112899203, -13.82090413600154299, 11.49999999999998934 ) ) ;
#46699=ORIENTED_EDGE ( 'NONE', *, *, #65753, .T. ) ;
#46702=CARTESIAN_POINT ( 'NONE',  ( -70.78956819130432621, -25.31392322340849432, 5.203679841770401104 ) ) ;
#46704=CARTESIAN_POINT ( 'NONE',  ( -51.62287095715005592, -23.48786465467241413, 11.44779295918254824 ) ) ;
#46706=CARTESIAN_POINT ( 'NONE',  ( -58.51505936317359158, -23.73791477778912196, 11.05961554403170588 ) ) ;
#46707=CARTESIAN_POINT ( 'NONE',  ( -115.6228709571500559, -23.47596703998600631, 11.44779298504227860 ) ) ;
#46708=CARTESIAN_POINT ( 'NONE',  ( -16.21995886604411297, 13.06735728859114509, -1.500000000000002220 ) ) ;
#46710=CARTESIAN_POINT ( 'NONE',  ( -19.00758693998263738, -10.61793046214600089, 11.49999999999999645 ) ) ;
#46711=DIRECTION ( 'NONE',  ( 1.000000000000000000, 3.773278334444167608E-23, 8.201307833595939069E-29 ) ) ;
#46712=CARTESIAN_POINT ( 'NONE',  ( -78.49838375731654594, -24.66019654487200441, 8.947790411086119278 ) ) ;
#46713=CARTESIAN_POINT ( 'NONE',  ( -16.74552829020559130, -14.98668287627115170, 11.49999999999998934 ) ) ;
#46714=CARTESIAN_POINT ( 'NONE',  ( -38.51306538520876188, -23.73766607897670511, -1.055555164236442689 ) ) ;
#46715=DIRECTION ( 'NONE',  ( 0.000000000000000000, 0.9999999999976377785, 2.173523156925979128E-06 ) ) ;
#46718=B_SPLINE_SURFACE_WITH_KNOTS ( 'NONE', 3, 3, ( 
 ( #36634, #84801, #45749, #46250 ),
 ( #99017, #76670, #60492, #7176 ),
 ( #44757, #83301, #75681, #92410 ),
 ( #98520, #6181, #22388, #38630 ),
 ( #29017, #73, #22881, #53372 ),
 ( #14784, #53869, #29513, #38125 ),
 ( #45255, #90423, #100005, #6679 ) ),
 .UNSPECIFIED., .F., .F., .F.,
 ( 4, 3, 4 ),
 ( 4, 4 ),
 ( 0.7945040050992240310, 0.8970133687736500105, 0.9995227324480759901 ),
 ( 0.4196006235780267435, 0.4208070636251879937 ),
 .UNSPECIFIED. ) ;
#46720=ORIENTED_EDGE ( 'NONE', *, *, #98973, .T. ) ;
#46721=ORIENTED_EDGE ( 'NONE', *, *, #79417, .T. ) ;
#46722=CARTESIAN_POINT ( 'NONE',  ( -10.68834330497911189, 18.46263264838738039, -1.500000000000002220 ) ) ;
#46724=CARTESIAN_POINT ( 'NONE',  ( -10.38599875782317206, -18.32754119035049101, -1.500000000000002220 ) ) ;
#46725=CARTESIAN_POINT ( 'NONE',  ( -30.54278559372614055, -24.67075338507718385, 1.095666116063849449 ) ) ;
#46726=CARTESIAN_POINT ( 'NONE',  ( -19.77041435686880533, -2.435487021107205940, -1.500000000000002220 ) ) ;
#46727=CARTESIAN_POINT ( 'NONE',  ( -99.58403181145372685, -25.24012543510424678, 3.741775170833818276 ) ) ;
#46729=CARTESIAN_POINT ( 'NONE',  ( -19.44315311050126382, -10.23602577120861667, -1.500000000000002220 ) ) ;
#46730=CARTESIAN_POINT ( 'NONE',  ( -68.62287095715005592, -23.47596703998600631, 11.44779298504227505 ) ) ;
#46731=ORIENTED_EDGE ( 'NONE', *, *, #60925, .T. ) ;
#46732=DIRECTION ( 'NONE',  ( 0.000000000000000000, 2.173523156925980399E-06, -0.9999999999976378895 ) ) ;
#46733=DIRECTION ( 'NONE',  ( 0.000000000000000000, -2.173523156925979552E-06, 0.9999999999976378895 ) ) ;
#46734=CARTESIAN_POINT ( 'NONE',  ( -5.376107494350208960, -20.15860285114975525, 11.49999999999999645 ) ) ;
#46738=PLANE ( 'NONE',  #48987 ) ;
#46739=FACE_OUTER_BOUND ( 'NONE', #22626, .T. ) ;
#46740=CARTESIAN_POINT ( 'NONE',  ( 11.00477826368897283, 18.22718707545001138, 11.49999999999998934 ) ) ;
#46741=CARTESIAN_POINT ( 'NONE',  ( -29.55620429048338949, -24.56885446186112532, 8.947790474426803087 ) ) ;
#46742=CARTESIAN_POINT ( 'NONE',  ( -107.5890161267547711, -24.35071581493543746, 9.817618358456021710 ) ) ;
#46743=EDGE_CURVE ( 'NONE', #1643, #25180, #38175, .T. ) ;
#46744=CARTESIAN_POINT ( 'NONE',  ( -69.86226385320381382, -29.50248914370730091, 2.832395270851967073 ) ) ;
#46746=CARTESIAN_POINT ( 'NONE',  ( -1.797493081057526032, -22.44471576765463183, -1.500000000000002220 ) ) ;
#46748=EDGE_LOOP ( 'NONE', ( #76028, #85352, #88396, #28468 ) ) ;
#46749=CARTESIAN_POINT ( 'NONE',  ( -89.62287095715002749, -23.48783264082478439, -1.443836473390063713 ) ) ;
#46750=CARTESIAN_POINT ( 'NONE',  ( -9.385407830382300531, 17.29636241635495608, 11.49999999999999645 ) ) ;
#46751=DIRECTION ( 'NONE',  ( -1.000000000000000000, -3.773278334444166432E-23, -8.201307841325785021E-29 ) ) ;
#46753=PLANE ( 'NONE',  #39869 ) ;
#46754=ORIENTED_EDGE ( 'NONE', *, *, #88374, .F. ) ;
#46756=CARTESIAN_POINT ( 'NONE',  ( -36.52287095715006870, -24.64965694238407323, 8.947790433994205372 ) ) ;
#46757=CARTESIAN_POINT ( 'NONE',  ( -89.90409546361829030, -25.12049752546737835, 2.832404795212227100 ) ) ;
#46759=CARTESIAN_POINT ( 'NONE',  ( 15.33752688427012778, 12.42672799324400934, 11.49999999999998934 ) ) ;
#46761=ORIENTED_EDGE ( 'NONE', *, *, #300, .T. ) ;
#46764=B_SPLINE_CURVE_WITH_KNOTS ( 'NONE', 3,
 ( #82757, #43709, #74645, #67062 ),
 .UNSPECIFIED., .F., .F.,
 ( 4, 4 ),
 ( 0.03878246734470643803, 0.03978321438547192945 ),
 .UNSPECIFIED. ) ;
#46767=FACE_OUTER_BOUND ( 'NONE', #19513, .T. ) ;
#46769=CARTESIAN_POINT ( 'NONE',  ( -55.63765809019586328, -24.52300882791528736, 0.6510814631126286001 ) ) ;
#46770=CARTESIAN_POINT ( 'NONE',  ( -98.94109201664207376, -25.03144944621345758, 6.485444833557155064 ) ) ;
#46771=CARTESIAN_POINT ( 'NONE',  ( -85.52287095715006160, -23.48783264082476663, -1.443836473390089470 ) ) ;
#46772=CARTESIAN_POINT ( 'NONE',  ( -91.94687923781920347, -25.22391124735684187, 6.409327647371628522 ) ) ;
#46773=CARTESIAN_POINT ( 'NONE',  ( -107.5130078572901766, -24.51314013834316086, 0.6176544820404228364 ) ) ;
#46774=CARTESIAN_POINT ( 'NONE',  ( 17.55240489776628721, -9.587225365216566431, 11.49999999999998934 ) ) ;
#46776=FACE_OUTER_BOUND ( 'NONE', #82650, .T. ) ;
#46777=ORIENTED_EDGE ( 'NONE', *, *, #4531, .F. ) ;
#46778=FACE_OUTER_BOUND ( 'NONE', #19096, .T. ) ;
#46779=CARTESIAN_POINT ( 'NONE',  ( -109.4679719608024300, -25.29012830856320093, 3.778970069853266445 ) ) ;
#46780=CARTESIAN_POINT ( 'NONE',  ( -120.6228709571500417, -24.92579138211019796, 1.929029949965668012 ) ) ;
#46781=CARTESIAN_POINT ( 'NONE',  ( -28.62287095715004881, -24.19626334920329214, 9.819127031579586884 ) ) ;
#46782=CARTESIAN_POINT ( 'NONE',  ( -38.62287095715005592, -23.48783264082477373, -1.443836473390072594 ) ) ;
#46783=CARTESIAN_POINT ( 'NONE',  ( -83.54731854358884391, -24.34968618360933590, 0.1864209137778810865 ) ) ;
#46784=B_SPLINE_SURFACE_WITH_KNOTS ( 'NONE', 3, 3, ( 
 ( #35398, #30825, #23197, #61790 ),
 ( #53676, #14086, #76481, #15589 ),
 ( #6987, #67905, #53176, #98826 ),
 ( #68393, #29820, #52666, #7984 ),
 ( #6491, #99808, #8491, #60791 ),
 ( #37442, #60293, #38933, #84106 ),
 ( #91217, #93214, #22690, #92217 ) ),
 .UNSPECIFIED., .F., .F., .F.,
 ( 4, 3, 4 ),
 ( 4, 4 ),
 ( 0.0004766839783815015100, 0.1029713700210894561, 0.2054660560637974198 ),
 ( 0.5196261812711125971, 0.5208786603924070446 ),
 .UNSPECIFIED. ) ;
#46787=VERTEX_POINT ( 'NONE', #100057 ) ;
#46790=VECTOR ( 'NONE', #72776, 1000.000000000000114 ) ;
#46791=CARTESIAN_POINT ( 'NONE',  ( 16.59675031405745571, -11.69241480613374407, -1.500000000000002220 ) ) ;
#46792=CARTESIAN_POINT ( 'NONE',  ( -109.6228709571500417, -23.48783264082478794, -1.443836473390060382 ) ) ;
#46793=EDGE_CURVE ( 'NONE', #86907, #98076, #53427, .T. ) ;
#46795=PLANE ( 'NONE',  #57366 ) ;
#46796=ADVANCED_FACE ( 'NONE', ( #13344 ), #5741, .T. ) ;
#46797=VERTEX_POINT ( 'NONE', #6237 ) ;
#46798=CARTESIAN_POINT ( 'NONE',  ( -86.52287095715006160, -23.48786465467241058, 11.44779295918254292 ) ) ;
#46799=CARTESIAN_POINT ( 'NONE',  ( 16.71511084712224360, -11.16500066668146829, -1.500000000000002220 ) ) ;
#46801=CARTESIAN_POINT ( 'NONE',  ( 18.35617536642501690, 10.39506492455470088, 11.49999999999999645 ) ) ;
#46803=CARTESIAN_POINT ( 'NONE',  ( -8.904070064990065703, -20.24664451029508783, -1.500000000000002220 ) ) ;
#46805=CARTESIAN_POINT ( 'NONE',  ( 4.502618398017903090, 20.03723546437915104, 11.49999999999998934 ) ) ;
#46807=ORIENTED_EDGE ( 'NONE', *, *, #50155, .T. ) ;
#46808=DIRECTION ( 'NONE',  ( -3.773278334453080206E-23, 0.9999999999976377785, 2.173523156925979975E-06 ) ) ;
#46810=CARTESIAN_POINT ( 'NONE',  ( -70.62287095715005592, -29.50250786944525672, 11.44777988621623699 ) ) ;
#46811=B_SPLINE_CURVE_WITH_KNOTS ( 'NONE', 3,
 ( #10177, #24393, #55363, #17285, #23888, #47241, #9169, #63487, #33019, #71083, #10679, #63994, #48248, #32009 ),
 .UNSPECIFIED., .F., .F.,
 ( 4, 2, 2, 2, 2, 2, 4 ),
 ( 0.000000000000000000, 0.0001575354624298309881, 0.0003150709248596619762, 0.0006301418497193228682, 0.0009452127745789835975, 0.001102748237008804259, 0.001260283699438624703 ),
 .UNSPECIFIED. ) ;
#46812=CARTESIAN_POINT ( 'NONE',  ( -110.6228709571500701, -23.48786465467241769, 11.44779295918254114 ) ) ;
#46816=B_SPLINE_CURVE_WITH_KNOTS ( 'NONE', 3,
 ( #767, #54558, #25094, #9876 ),
 .UNSPECIFIED., .F., .F.,
 ( 4, 4 ),
 ( 0.000000000000000000, 1.000000000000000000 ),
 .UNSPECIFIED. ) ;
#46819=CARTESIAN_POINT ( 'NONE',  ( -49.54700823480037997, -25.07535432491515692, 7.358156397503878843 ) ) ;
#46821=CARTESIAN_POINT ( 'NONE',  ( 0.06016934085327452914, 20.63536315578604174, -1.500000000000002220 ) ) ;
#46822=CARTESIAN_POINT ( 'NONE',  ( 7.401388779597747103, 20.28278527911644247, 11.49999999999999645 ) ) ;
#46824=CARTESIAN_POINT ( 'NONE',  ( -83.62287095715002749, -23.94994826722515668, -0.6494450866351706431 ) ) ;
#46826=CARTESIAN_POINT ( 'NONE',  ( 3.152853332073482839, 22.16862046936333286, 11.49999999999998934 ) ) ;
#46827=ADVANCED_FACE ( 'NONE', ( #61543 ), #53925, .F. ) ;
#46828=DIRECTION ( 'NONE',  ( -3.773278334453079030E-23, 0.9999999999976377785, 2.173523156925979128E-06 ) ) ;
#46829=PLANE ( 'NONE',  #72404 ) ;
#46830=ORIENTED_EDGE ( 'NONE', *, *, #100082, .T. ) ;
#46831=CARTESIAN_POINT ( 'NONE',  ( -99.57937527035555547, -25.29211892742296541, 4.244792190146649880 ) ) ;
#46832=CARTESIAN_POINT ( 'NONE',  ( -67.62287095715005592, -23.48786465467241058, 11.44779295918254647 ) ) ;
#46833=CARTESIAN_POINT ( 'NONE',  ( -0.7727808018759799724, -20.89725122839497828, 11.49999999999998934 ) ) ;
#46835=CARTESIAN_POINT ( 'NONE',  ( -120.6228709571500417, -29.50248789122583659, 2.256150453626215580 ) ) ;
#46837=CARTESIAN_POINT ( 'NONE',  ( -109.5126105237879841, -24.66019654487200441, 8.947790411086113949 ) ) ;
#46838=CARTESIAN_POINT ( 'NONE',  ( -17.86006801910157193, 11.38285951858322242, -1.500000000000002220 ) ) ;
#46840=CARTESIAN_POINT ( 'NONE',  ( -50.63860451389618333, -24.52300882791530157, 0.6510814631126389251 ) ) ;
#46841=CARTESIAN_POINT ( 'NONE',  ( 10.97640485992876691, 18.82695874702771377, -1.500000000000002220 ) ) ;
#46842=CARTESIAN_POINT ( 'NONE',  ( -121.5228709571500332, -23.73934037231757443, 11.05740245334328087 ) ) ;
#46843=DIRECTION ( 'NONE',  ( -3.773278334453079618E-23, 0.9999999999976377785, 2.173523156925979975E-06 ) ) ;
#46844=LINE ( 'NONE', #85389, #88663 ) ;
#46845=CARTESIAN_POINT ( 'NONE',  ( 21.63681353182189682, 2.665401433100548889, -1.500000000000002220 ) ) ;
#46847=ORIENTED_EDGE ( 'NONE', *, *, #94638, .F. ) ;
#46853=CARTESIAN_POINT ( 'NONE',  ( -28.04362312726946271, -24.81012858093322038, 2.323251710168637185 ) ) ;
#46854=CARTESIAN_POINT ( 'NONE',  ( -44.62287095715004881, -23.72747288104469732, -1.053458166803227458 ) ) ;
#46855=CARTESIAN_POINT ( 'NONE',  ( 7.993063233546146229, -19.64520799392144568, 11.49999999999998934 ) ) ;
#46856=CARTESIAN_POINT ( 'NONE',  ( -94.51552831490990059, -23.96119346886881019, -0.6495511937832051386 ) ) ;
#46857=CARTESIAN_POINT ( 'NONE',  ( -95.62287095715005592, -23.47596703998600631, 11.44779298504227860 ) ) ;
#46858=CARTESIAN_POINT ( 'NONE',  ( -80.48900664166535535, -25.13313949306887807, 7.101635536975466678 ) ) ;
#46860=CARTESIAN_POINT ( 'NONE',  ( 7.147005326088517130, -18.03964237587283037, 11.49999999999998934 ) ) ;
#46861=ADVANCED_FACE ( 'NONE', ( #77227 ), #91467, .F. ) ;
#46862=CARTESIAN_POINT ( 'NONE',  ( -39.98075019704535293, -25.25978494880519776, 3.590542803917028181 ) ) ;
#46864=VECTOR ( 'NONE', #4378, 1000.000000000000114 ) ;
#46865=CARTESIAN_POINT ( 'NONE',  ( -14.69715086760845857, -12.76062437926726290, 11.49999999999999645 ) ) ;
#46867=AXIS2_PLACEMENT_3D ( 'NONE', #98891, #61353, #7049 ) ;
#46868=CARTESIAN_POINT ( 'NONE',  ( -107.5228709571500758, -24.65952944569304961, 1.056160979905704123 ) ) ;
#46870=VERTEX_POINT ( 'NONE', #98580 ) ;
#46871=CARTESIAN_POINT ( 'NONE',  ( -93.62287095715004170, -23.94994826722515668, -0.6494450866351687557 ) ) ;
#46873=B_SPLINE_CURVE_WITH_KNOTS ( 'NONE', 3,
 ( #33315, #25203, #371, #56181, #87106, #31318, #70897, #63295, #48572, #79496, #64302, #25706, #35333, #3395, #49564, #26214 ),
 .UNSPECIFIED., .F., .F.,
 ( 4, 2, 2, 2, 2, 2, 2, 4 ),
 ( 0.000000000000000000, 0.0002741513364169689197, 0.0005483026728339378394, 0.0008224540092509068133, 0.001096605345667875679, 0.001644908018501813627, 0.001919059354918762651, 0.002193210691335711893 ),
 .UNSPECIFIED. ) ;
#46875=CARTESIAN_POINT ( 'NONE',  ( -93.50526767657690641, -24.66019654487200441, 8.947790411086105067 ) ) ;
#46876=CARTESIAN_POINT ( 'NONE',  ( 19.42422255247381457, -2.945173967302487039, 11.49999999999998934 ) ) ;
#46879=VERTEX_POINT ( 'NONE', #60050 ) ;
#46880=CARTESIAN_POINT ( 'NONE',  ( 18.62697458635512859, 10.92912097662538251, -1.500000000000002220 ) ) ;
#46882=CARTESIAN_POINT ( 'NONE',  ( -40.60175827569378981, -24.15503026093912453, -0.2815557561904605266 ) ) ;
#46884=CARTESIAN_POINT ( 'NONE',  ( -15.77545706029219730, -16.76941864122914083, -1.500000000000002220 ) ) ;
#46887=FACE_OUTER_BOUND ( 'NONE', #90157, .T. ) ;
#46889=CARTESIAN_POINT ( 'NONE',  ( -40.85509153498097845, -25.20774029359534296, 6.732786232439175400 ) ) ;
#46890=CARTESIAN_POINT ( 'NONE',  ( -101.8274488899549368, -25.20041407164857361, 6.674697471738888943 ) ) ;
#46891=CARTESIAN_POINT ( 'NONE',  ( -110.6079876523469920, -25.10921379075584525, 2.855977848569461575 ) ) ;
#46892=CARTESIAN_POINT ( 'NONE',  ( -121.6228709571500275, -24.66019654487200441, 8.947790411086119278 ) ) ;
#46893=CARTESIAN_POINT ( 'NONE',  ( -99.25286268653823640, -25.26400796470216292, 4.527133510428875240 ) ) ;
#46894=CARTESIAN_POINT ( 'NONE',  ( 15.94990109002195489, -11.90149544800030590, 11.49999999999998934 ) ) ;
#46895=CARTESIAN_POINT ( 'NONE',  ( -101.2870029445573010, -25.25608464488718496, 3.797624798826384040 ) ) ;
#46896=CARTESIAN_POINT ( 'NONE',  ( -7.754168067426306266, 18.25094163199162622, -1.500000000000002220 ) ) ;
#46898=CARTESIAN_POINT ( 'NONE',  ( -39.57984969116796492, -25.29116578775463964, 3.109569074945083944 ) ) ;
#46899=CARTESIAN_POINT ( 'NONE',  ( -42.52287095715006870, -23.94994826722564696, -0.6494450866342741380 ) ) ;
#46900=CARTESIAN_POINT ( 'NONE',  ( -19.59449498831206782, -6.737714454370689054, 11.49999999999999645 ) ) ;
#46902=CARTESIAN_POINT ( 'NONE',  ( -78.52287095715007581, -23.72773821059536914, 11.05748984161097503 ) ) ;
#46903=VECTOR ( 'NONE', #41166, 1000.000000000000114 ) ;
#46904=CARTESIAN_POINT ( 'NONE',  ( 20.42703387425654427, 10.12935691860780985, 11.49999999999999645 ) ) ;
#46905=ORIENTED_EDGE ( 'NONE', *, *, #88074, .T. ) ;
#46906=FACE_OUTER_BOUND ( 'NONE', #89273, .T. ) ;
#46909=CARTESIAN_POINT ( 'NONE',  ( -16.67386609800740516, 11.36076560755915033, 11.49999999999998934 ) ) ;
#46910=B_SPLINE_CURVE_WITH_KNOTS ( 'NONE', 3,
 ( #92073, #22544, #14944, #5351, #5847, #45915 ),
 .UNSPECIFIED., .F., .F.,
 ( 4, 2, 4 ),
 ( 0.000000000000000000, 0.001380764517854764532, 0.002761529035709529064 ),
 .UNSPECIFIED. ) ;
#46912=CARTESIAN_POINT ( 'NONE',  ( -69.58953762381672448, -23.48783264082478084, -1.443836473390067265 ) ) ;
#46913=VERTEX_POINT ( 'NONE', #90977 ) ;
#46914=ORIENTED_EDGE ( 'NONE', *, *, #7154, .T. ) ;
#46916=CARTESIAN_POINT ( 'NONE',  ( 7.980177114813061579, 21.45908683785374649, 11.49999999999998934 ) ) ;
#46917=CARTESIAN_POINT ( 'NONE',  ( -41.86995616089614458, -25.28979658489737048, 4.210709715701590028 ) ) ;
#46918=CARTESIAN_POINT ( 'NONE',  ( 11.52859134480388903, -18.33581920571378632, -1.500000000000002220 ) ) ;
#46920=EDGE_CURVE ( 'NONE', #56862, #94573, #95923, .T. ) ;
#46921=CARTESIAN_POINT ( 'NONE',  ( 20.33208665566141704, 4.825383418962623239, 11.49999999999999645 ) ) ;
#46923=CARTESIAN_POINT ( 'NONE',  ( -69.42561217104606897, -25.24754309793884843, 5.145891976043102112 ) ) ;
#46924=CARTESIAN_POINT ( 'NONE',  ( -7.807709442696729063, 20.60712426125841645, 11.49999999999998934 ) ) ;
#46928=CARTESIAN_POINT ( 'NONE',  ( -65.62287095715005592, -24.99156045073393173, 7.747789690856161648 ) ) ;
#46930=CARTESIAN_POINT ( 'NONE',  ( -49.56515190845122021, -25.18440198093164639, 3.736414966849777475 ) ) ;
#46931=CARTESIAN_POINT ( 'NONE',  ( -46.52287095715007581, -23.48783264082477018, -1.443836473390096797 ) ) ;
#46932=ORIENTED_EDGE ( 'NONE', *, *, #96086, .F. ) ;
#46934=ORIENTED_EDGE ( 'NONE', *, *, #47154, .F. ) ;
#46937=CARTESIAN_POINT ( 'NONE',  ( -106.6228709571500559, -24.65952944569304606, 1.056160979905703012 ) ) ;
#46941=B_SPLINE_CURVE_WITH_KNOTS ( 'NONE', 3,
 ( #56513, #54632, #41274, #57014, #17935, #79822, #15052, #46024 ),
 .UNSPECIFIED., .F., .F.,
 ( 4, 2, 2, 4 ),
 ( -0.001224554619866339558, -0.0002241820295893590283, 0.0007761905606876215013, 0.002776935741241573670 ),
 .UNSPECIFIED. ) ;
#46942=CARTESIAN_POINT ( 'NONE',  ( 6.539103723289373171, -19.38406401830294712, -1.500000000000002220 ) ) ;
#46944=CARTESIAN_POINT ( 'NONE',  ( -79.52287095715010423, -23.47593901973090524, -1.443836447538996870 ) ) ;
#46946=CARTESIAN_POINT ( 'NONE',  ( -62.52287095715006160, -23.48783264082477018, -1.443836473390091912 ) ) ;
#46947=CARTESIAN_POINT ( 'NONE',  ( -77.58953762381673869, -24.64898659630367916, 1.056161002820385830 ) ) ;
#46948=CARTESIAN_POINT ( 'NONE',  ( 20.80681148587913754, 8.022540738981085440, 11.49999999999998934 ) ) ;
#46950=CARTESIAN_POINT ( 'NONE',  ( -124.6228709571500559, -29.50247984919015209, -1.443849546365046699 ) ) ;
#46951=EDGE_LOOP ( 'NONE', ( #98462, #64078, #84825, #97493, #34839, #43328, #10529, #29578 ) ) ;
#46953=VECTOR ( 'NONE', #11132, 1000.000000000000114 ) ;
#46954=PLANE ( 'NONE',  #81549 ) ;
#46956=CARTESIAN_POINT ( 'NONE',  ( -4.186882374726557110, 20.40937146592452223, -1.500000000000002220 ) ) ;
#46958=DIRECTION ( 'NONE',  ( -3.773278334453079030E-23, 0.9999999999976377785, 2.173523156925979128E-06 ) ) ;
#46959=EDGE_LOOP ( 'NONE', ( #3793, #75899, #42937, #44100 ) ) ;
#46960=VERTEX_POINT ( 'NONE', #2148 ) ;
#46961=AXIS2_PLACEMENT_3D ( 'NONE', #13005, #43482, #43971 ) ;
#46962=CARTESIAN_POINT ( 'NONE',  ( -58.52287095715006160, -24.64965694238407323, 8.947790433994201820 ) ) ;
#46963=CARTESIAN_POINT ( 'NONE',  ( 8.737904895026865404, 19.08465823478955414, -1.500000000000002220 ) ) ;
#46964=ORIENTED_EDGE ( 'NONE', *, *, #7401, .T. ) ;
#46965=CARTESIAN_POINT ( 'NONE',  ( -110.6228709571500275, -24.91544648472627088, 1.928969306349440194 ) ) ;
#46968=CARTESIAN_POINT ( 'NONE',  ( -51.58953762381673158, -24.65952944569304606, 1.056160979905695463 ) ) ;
#46969=CARTESIAN_POINT ( 'NONE',  ( -92.55803716275170245, -23.73791477778912196, 11.05961554403170588 ) ) ;
#46970=CARTESIAN_POINT ( 'NONE',  ( -119.6228709571500559, -23.48783264082479150, -1.443836473390058384 ) ) ;
#46971=CARTESIAN_POINT ( 'NONE',  ( -21.91774099701738621, 3.392077650570975766, 11.49999999999999645 ) ) ;
#46973=DIRECTION ( 'NONE',  ( -3.773278334453079618E-23, 0.9999999999976377785, 2.173523156925979975E-06 ) ) ;
#46974=PLANE ( 'NONE',  #91002 ) ;
#46976=CARTESIAN_POINT ( 'NONE',  ( -16.08347380570801377, -15.98036338121420030, -1.500000000000002220 ) ) ;
#46979=EDGE_CURVE ( 'NONE', #42205, #92012, #80101, .T. ) ;
#46982=ADVANCED_FACE ( 'NONE', ( #31570 ), #31065, .T. ) ;
#46983=CARTESIAN_POINT ( 'NONE',  ( 19.96388892861992659, -2.714421270036905032, 11.49999999999998934 ) ) ;
#46987=CARTESIAN_POINT ( 'NONE',  ( -5.491053050139323766, 21.65304554001118120, -1.500000000000002220 ) ) ;
#46989=VERTEX_POINT ( 'NONE', #87360 ) ;
#46990=CARTESIAN_POINT ( 'NONE',  ( -101.4810573493621177, -25.16257346776554371, 6.435289059764511599 ) ) ;
#46991=CARTESIAN_POINT ( 'NONE',  ( -89.62287095715002749, -24.50321055353805022, 9.387540953477527594 ) ) ;
#46992=CARTESIAN_POINT ( 'NONE',  ( -65.62287095715005592, -25.00158670708909270, 2.256160236439166855 ) ) ;
#46994=CARTESIAN_POINT ( 'NONE',  ( -97.25593758936675215, -24.04615231314291890, -0.4716817114508916609 ) ) ;
#46995=CARTESIAN_POINT ( 'NONE',  ( -13.18904525526904692, 14.46673508071025971, -1.500000000000002220 ) ) ;
#46996=DIRECTION ( 'NONE',  ( -3.773278334453079618E-23, 0.9999999999976377785, 2.173523156925979975E-06 ) ) ;
#46997=CARTESIAN_POINT ( 'NONE',  ( 17.49997855696484095, 12.48231381050728928, 11.49999999999998934 ) ) ;
#46998=CARTESIAN_POINT ( 'NONE',  ( -128.5215775092486865, -24.34968618360935011, 0.1864209137779018477 ) ) ;
#47003=CARTESIAN_POINT ( 'NONE',  ( 17.53461989915211916, -14.66684187699354425, -1.500000000000002220 ) ) ;
#47006=B_SPLINE_CURVE_WITH_KNOTS ( 'NONE', 3,
 ( #52145, #51650, #20680, #13564 ),
 .UNSPECIFIED., .F., .F.,
 ( 4, 4 ),
 ( 0.000000000000000000, 0.0001000000000000028644 ),
 .UNSPECIFIED. ) ;
#47008=PLANE ( 'NONE',  #49935 ) ;
#47009=DIRECTION ( 'NONE',  ( 0.000000000000000000, -0.9999999999976377785, -2.173523156925979975E-06 ) ) ;
#47010=CARTESIAN_POINT ( 'NONE',  ( -8.782848147209532996, 18.00178819457707746, 11.49999999999999645 ) ) ;
#47011=CARTESIAN_POINT ( 'NONE',  ( -78.94303308397306296, -25.31594635886830957, 5.977536581945547489 ) ) ;
#47014=B_SPLINE_CURVE_WITH_KNOTS ( 'NONE', 3,
 ( #388, #16108, #45579, #67921 ),
 .UNSPECIFIED., .F., .F.,
 ( 4, 4 ),
 ( 0.000000000000000000, 0.0001000000000000028644 ),
 .UNSPECIFIED. ) ;
#47015=DIRECTION ( 'NONE',  ( 0.000000000000000000, 2.173523156893721996E-06, -0.9999999999976377785 ) ) ;
#47016=LINE ( 'NONE', #62755, #52144 ) ;
#47018=CARTESIAN_POINT ( 'NONE',  ( -110.6228709571500559, -23.47593901973091235, -1.443836447538999312 ) ) ;
#47019=CARTESIAN_POINT ( 'NONE',  ( 9.899741330608472722, -19.37759744025533593, 11.49999999999998934 ) ) ;
#47020=ADVANCED_FACE ( 'NONE', ( #39682 ), #69646, .F. ) ;
#47021=DIRECTION ( 'NONE',  ( 1.000000000000000000, 3.773278334444167608E-23, 8.201307833595939069E-29 ) ) ;
#47023=CARTESIAN_POINT ( 'NONE',  ( -19.15281226579456231, 4.489446101945751444, -1.500000000000002220 ) ) ;
#47024=CARTESIAN_POINT ( 'NONE',  ( -38.58953762381672448, -23.48786465467240703, 11.44779295918255180 ) ) ;
#47026=CARTESIAN_POINT ( 'NONE',  ( -41.46019029217195850, -25.26930233494256584, 4.061970619173578712 ) ) ;
#47028=VECTOR ( 'NONE', #63935, 1000.000000000000114 ) ;
#47029=CARTESIAN_POINT ( 'NONE',  ( -91.59147232029850727, -24.15620529776628445, 10.23563542870660115 ) ) ;
#47031=CARTESIAN_POINT ( 'NONE',  ( 1.511266892140219920, 20.53031905857337591, 11.49999999999999645 ) ) ;
#47033=CARTESIAN_POINT ( 'NONE',  ( -120.5543864198989183, -24.40034930558991633, 0.3402023900116107336 ) ) ;
#47034=VECTOR ( 'NONE', #18899, 1000.000000000000114 ) ;
#47035=CARTESIAN_POINT ( 'NONE',  ( 22.48748499206561746, 2.281147167042596013, 11.49999999999999645 ) ) ;
#47036=ORIENTED_EDGE ( 'NONE', *, *, #21959, .F. ) ;
#47037=CARTESIAN_POINT ( 'NONE',  ( -100.0631793594960044, -25.26387431326939037, 4.632689007454804830 ) ) ;
#47038=CARTESIAN_POINT ( 'NONE',  ( -60.58953762381673158, -24.99132157543084531, 2.256160258750496972 ) ) ;
#47039=VECTOR ( 'NONE', #17095, 1000.000000000000114 ) ;
#47040=CARTESIAN_POINT ( 'NONE',  ( -125.6257034592155861, -23.85049219812686516, 10.88485053497526778 ) ) ;
#47042=EDGE_CURVE ( 'NONE', #53195, #41736, #7486, .T. ) ;
#47043=CARTESIAN_POINT ( 'NONE',  ( -26.14934357328621317, -24.61459939561487786, 7.450065485979896707 ) ) ;
#47046=CARTESIAN_POINT ( 'NONE',  ( -8.497478458550677516, -21.44862750780143656, 11.49999999999999645 ) ) ;
#47047=B_SPLINE_CURVE_WITH_KNOTS ( 'NONE', 3,
 ( #57779, #87723, #89218, #3491 ),
 .UNSPECIFIED., .F., .F.,
 ( 4, 4 ),
 ( 0.2499644179499421748, 0.2589708492220576530 ),
 .UNSPECIFIED. ) ;
#47048=CARTESIAN_POINT ( 'NONE',  ( 19.59772090806136902, -11.66877021596143926, 11.49999999999998934 ) ) ;
#47049=PLANE ( 'NONE',  #59998 ) ;
#47050=CARTESIAN_POINT ( 'NONE',  ( -96.55782209890644197, -23.73766607897670511, -1.055555164236452681 ) ) ;
#47051=FACE_OUTER_BOUND ( 'NONE', #62849, .T. ) ;
#47052=CARTESIAN_POINT ( 'NONE',  ( 21.09243369641204069, 7.689775423913054908, 11.49999999999999645 ) ) ;
#47055=B_SPLINE_CURVE_WITH_KNOTS ( 'NONE', 3,
 ( #98120, #29614, #68190, #36246 ),
 .UNSPECIFIED., .F., .F.,
 ( 4, 4 ),
 ( 0.000000000000000000, 1.000000000000000000 ),
 .UNSPECIFIED. ) ;
#47056=CARTESIAN_POINT ( 'NONE',  ( -34.62287095715005592, -23.95044443724991368, 10.65354141964650303 ) ) ;
#47057=CARTESIAN_POINT ( 'NONE',  ( 15.37660858059359725, 15.65766701038582021, -1.500000000000002220 ) ) ;
#47058=EDGE_CURVE ( 'NONE', #79151, #77983, #78727, .T. ) ;
#47061=CARTESIAN_POINT ( 'NONE',  ( -74.62287095715005592, -23.48786465467241058, 11.44779295918254469 ) ) ;
#47066=CARTESIAN_POINT ( 'NONE',  ( -3.437008290023895185, 20.19323497536227663, 11.49999999999998934 ) ) ;
#47067=ORIENTED_EDGE ( 'NONE', *, *, #11877, .F. ) ;
#47069=ORIENTED_EDGE ( 'NONE', *, *, #54638, .T. ) ;
#47070=ORIENTED_EDGE ( 'NONE', *, *, #55328, .F. ) ;
#47071=CARTESIAN_POINT ( 'NONE',  ( -10.32085834726444595, 20.65377284989807194, 11.49999999999998934 ) ) ;
#47072=CARTESIAN_POINT ( 'NONE',  ( -49.98363062963033343, -25.13033135890777459, 2.887186111250463760 ) ) ;
#47073=EDGE_CURVE ( 'NONE', #95103, #32116, #15925, .T. ) ;
#47074=CARTESIAN_POINT ( 'NONE',  ( -3.904290608643684379, -19.93223805144805283, -1.500000000000002220 ) ) ;
#47077=CARTESIAN_POINT ( 'NONE',  ( -92.59760823315281186, -23.73766607897671221, -1.055555164236430477 ) ) ;
#47079=CARTESIAN_POINT ( 'NONE',  ( -39.62287095715005592, -23.47596703998600276, 11.44779298504227505 ) ) ;
#47081=CARTESIAN_POINT ( 'NONE',  ( -21.26083644630951142, -3.357327265692296780, 11.49999999999999645 ) ) ;
#47082=ORIENTED_EDGE ( 'NONE', *, *, #66649, .T. ) ;
#47083=FACE_OUTER_BOUND ( 'NONE', #42652, .T. ) ;
#47085=ORIENTED_EDGE ( 'NONE', *, *, #44738, .T. ) ;
#47086=CARTESIAN_POINT ( 'NONE',  ( -14.15296684469643118, 15.14645709676483420, -1.500000000000002220 ) ) ;
#47090=ORIENTED_EDGE ( 'NONE', *, *, #44413, .T. ) ;
#47091=CARTESIAN_POINT ( 'NONE',  ( -41.58131642490323543, -24.51419770103157347, 9.386484678747180510 ) ) ;
#47095=CARTESIAN_POINT ( 'NONE',  ( -28.52287095715005805, -24.49960542107631056, 8.947790409070465856 ) ) ;
#47096=CARTESIAN_POINT ( 'NONE',  ( -77.62287095715005592, -24.50321055353804667, 9.387540953477524042 ) ) ;
#47098=CARTESIAN_POINT ( 'NONE',  ( -14.32918165687622825, -16.72005635474405949, 11.49999999999999645 ) ) ;
#47100=CARTESIAN_POINT ( 'NONE',  ( -3.310667818835141940, 22.29536907041311977, 11.49999999999998934 ) ) ;
#47101=CARTESIAN_POINT ( 'NONE',  ( -7.324709186033012465, -19.69651249574825513, 11.49999999999998934 ) ) ;
#47103=CARTESIAN_POINT ( 'NONE',  ( -70.52287095715007581, -29.50250243563736774, 8.947779886222143375 ) ) ;
#47104=ORIENTED_EDGE ( 'NONE', *, *, #77018, .T. ) ;
#47105=VECTOR ( 'NONE', #99136, 1000.000000000000114 ) ;
#47106=B_SPLINE_CURVE_WITH_KNOTS ( 'NONE', 3,
 ( #50417, #89967, #74729, #66664, #34193, #81361 ),
 .UNSPECIFIED., .F., .F.,
 ( 4, 2, 4 ),
 ( 0.000000000000000000, 0.001380764517854769953, 0.002761529035709539906 ),
 .UNSPECIFIED. ) ;
#47109=CARTESIAN_POINT ( 'NONE',  ( -77.62287095715005592, -29.50248528299804818, 1.056150453629038477 ) ) ;
#47113=ORIENTED_EDGE ( 'NONE', *, *, #25399, .F. ) ;
#47114=CARTESIAN_POINT ( 'NONE',  ( 10.98566517548414012, -18.08203305749968592, 11.49999999999998934 ) ) ;
#47115=CARTESIAN_POINT ( 'NONE',  ( -126.6228709571500559, -24.34917612406838927, 0.1852690917426733086 ) ) ;
#47116=CARTESIAN_POINT ( 'NONE',  ( -51.87944994387085274, -25.03148522597936321, 6.553577993683898484 ) ) ;
#47117=CARTESIAN_POINT ( 'NONE',  ( -121.5181200719720493, -24.65952944569305316, 1.056160979905709008 ) ) ;
#47118=DIRECTION ( 'NONE',  ( 0.000000000000000000, 0.9999999999976377785, 2.173523156925979975E-06 ) ) ;
#47120=CARTESIAN_POINT ( 'NONE',  ( -10.57539506955483333, 19.50334513348995813, -1.500000000000002220 ) ) ;
#47124=CARTESIAN_POINT ( 'NONE',  ( -37.60901958438072512, -23.73766607897671221, -1.055555164236442023 ) ) ;
#47125=CARTESIAN_POINT ( 'NONE',  ( -40.45206973576002696, -25.30357236805550158, 5.543059975338419321 ) ) ;
#47128=CARTESIAN_POINT ( 'NONE',  ( 4.201609111248720829, -18.99613120386805676, 11.49999999999998934 ) ) ;
#47129=CARTESIAN_POINT ( 'NONE',  ( -20.78045986758521835, -5.208592277829342088, 11.49999999999998934 ) ) ;
#47130=CARTESIAN_POINT ( 'NONE',  ( -62.57945775862675220, -24.65952944569303895, 1.056160979905693686 ) ) ;
#47132=DIRECTION ( 'NONE',  ( 1.000000000000000000, 3.773278334444166432E-23, 8.201307841325785021E-29 ) ) ;
#47134=CARTESIAN_POINT ( 'NONE',  ( -14.80616194778269623, -17.16973004002414882, -1.500000000000002220 ) ) ;
#47136=EDGE_CURVE ( 'NONE', #89504, #88443, #55426, .T. ) ;
#47137=CARTESIAN_POINT ( 'NONE',  ( -118.5228709571500758, -29.50250243563736774, 8.947779886222134493 ) ) ;
#47138=PLANE ( 'NONE',  #58981 ) ;
#47139=CARTESIAN_POINT ( 'NONE',  ( 8.478510716907816658, 17.93336729499101523, 11.49999999999999645 ) ) ;
#47141=CARTESIAN_POINT ( 'NONE',  ( -108.5228709571500616, -23.48786465467241769, 11.44779295918253936 ) ) ;
#47142=CARTESIAN_POINT ( 'NONE',  ( -50.92287095715006018, -23.47593901973090169, -1.443836447538997980 ) ) ;
#47145=CARTESIAN_POINT ( 'NONE',  ( -80.52287095715004739, -24.51254535375850807, 9.355368624242062836 ) ) ;
#47146=CARTESIAN_POINT ( 'NONE',  ( -51.60452015029387951, -25.27412385504897685, 3.558372972795847744 ) ) ;
#47147=CARTESIAN_POINT ( 'NONE',  ( -5.395268184683536639, 21.00466093859614958, 11.49999999999998934 ) ) ;
#47148=EDGE_CURVE ( 'NONE', #13751, #51301, #12332, .T. ) ;
#47149=CARTESIAN_POINT ( 'NONE',  ( -124.5895376238167103, -24.64898659630368627, 1.056161002820393158 ) ) ;
#47150=CARTESIAN_POINT ( 'NONE',  ( 9.746180923669104601, -16.83516941858706417, -1.500000000000002220 ) ) ;
#47151=EDGE_CURVE ( 'NONE', #22015, #53195, #94654, .T. ) ;
#47152=CARTESIAN_POINT ( 'NONE',  ( -123.6228709571500701, -24.51387760970725083, 9.387446482453407626 ) ) ;
#47153=ORIENTED_EDGE ( 'NONE', *, *, #32854, .F. ) ;
#47154=EDGE_CURVE ( 'NONE', #5356, #29214, #71656, .T. ) ;
#47155=CARTESIAN_POINT ( 'NONE',  ( -14.79517943714664518, -13.99575967537150412, 11.49999999999999645 ) ) ;
#47156=CARTESIAN_POINT ( 'NONE',  ( -80.50192592861780838, -24.52300882791530157, 0.6510814631126378149 ) ) ;
#47158=ORIENTED_EDGE ( 'NONE', *, *, #60800, .T. ) ;
#47159=CARTESIAN_POINT ( 'NONE',  ( -40.45829750704997707, -25.19502912051678223, 3.293943094755625633 ) ) ;
#47160=CARTESIAN_POINT ( 'NONE',  ( -61.64687923781919920, -25.14083923594766645, 2.947789366383931853 ) ) ;
#47161=CARTESIAN_POINT ( 'NONE',  ( -40.52319934060825091, -24.92592662359560762, 8.075495903017996469 ) ) ;
#47163=CARTESIAN_POINT ( 'NONE',  ( 17.00595499256408871, 10.69956108467327205, -1.500000000000002220 ) ) ;
#47164=ADVANCED_FACE ( 'NONE', ( #65062 ), #89366, .T. ) ;
#47166=ORIENTED_EDGE ( 'NONE', *, *, #15465, .T. ) ;
#47168=B_SPLINE_CURVE_WITH_KNOTS ( 'NONE', 3,
 ( #94808, #47152, #70482, #39529, #56276, #63390 ),
 .UNSPECIFIED., .F., .F.,
 ( 4, 2, 4 ),
 ( 1.570887131794333942E-05, 0.001396322306279761073, 0.002776935741241578874 ),
 .UNSPECIFIED. ) ;
#47170=CARTESIAN_POINT ( 'NONE',  ( -13.69284064830502423, 18.33895024417757469, 11.49999999999999645 ) ) ;
#47171=CARTESIAN_POINT ( 'NONE',  ( 4.564784964189898098, -22.25151590922551748, 11.49999999999998934 ) ) ;
#47173=CARTESIAN_POINT ( 'NONE',  ( -71.64150769953161557, -25.20622457644260805, 6.632340821967897426 ) ) ;
#47174=CARTESIAN_POINT ( 'NONE',  ( -114.5228709571500616, -23.47596703998600631, 11.44779298504228038 ) ) ;
#47176=CARTESIAN_POINT ( 'NONE',  ( -73.55620429048340725, -23.48783264082478084, -1.443836473390067265 ) ) ;
#47177=EDGE_CURVE ( 'NONE', #88166, #47537, #4136, .T. ) ;
#47178=CARTESIAN_POINT ( 'NONE',  ( -128.6241757553235345, -23.73791477778912196, 11.05961554403169522 ) ) ;
#47179=ADVANCED_FACE ( 'NONE', ( #41201 ), #15165, .T. ) ;
#47180=CARTESIAN_POINT ( 'NONE',  ( -98.89396085167129513, -25.25460717992483950, 6.074556580732870970 ) ) ;
#47182=CARTESIAN_POINT ( 'NONE',  ( 20.35419724272142616, 1.316291261081859787, -1.500000000000002220 ) ) ;
#47184=CARTESIAN_POINT ( 'NONE',  ( 12.94906671069258763, 19.00495796004926419, -1.500000000000002220 ) ) ;
#47186=EDGE_CURVE ( 'NONE', #39879, #58273, #41480, .T. ) ;
#47188=VERTEX_POINT ( 'NONE', #60313 ) ;
#47189=CARTESIAN_POINT ( 'NONE',  ( -108.5964301896317892, -23.48786465467241413, 11.44779295918253759 ) ) ;
#47191=EDGE_CURVE ( 'NONE', #56219, #90373, #75231, .T. ) ;
#47193=CARTESIAN_POINT ( 'NONE',  ( 5.124585555570928541, 20.71496159572455653, 11.49999999999999645 ) ) ;
#47195=ORIENTED_EDGE ( 'NONE', *, *, #67363, .T. ) ;
#47196=CARTESIAN_POINT ( 'NONE',  ( -22.22723998432330106, 0.1330083165726352878, 11.49999999999998934 ) ) ;
#47197=CARTESIAN_POINT ( 'NONE',  ( -6.358105417860958397, -19.66046682221446318, -1.500000000000002220 ) ) ;
#47198=ORIENTED_EDGE ( 'NONE', *, *, #13626, .T. ) ;
#47200=B_SPLINE_CURVE_WITH_KNOTS ( 'NONE', 3,
 ( #57638, #18555, #95186, #56641, #48526, #49528 ),
 .UNSPECIFIED., .F., .F.,
 ( 4, 2, 4 ),
 ( 0.000000000000000000, 0.001380901958385390930, 0.002761803916770781860 ),
 .UNSPECIFIED. ) ;
#47201=CARTESIAN_POINT ( 'NONE',  ( -95.50150560350351725, -25.00182538069147142, 7.747789668545043362 ) ) ;
#47202=ORIENTED_EDGE ( 'NONE', *, *, #89531, .F. ) ;
#47203=CARTESIAN_POINT ( 'NONE',  ( -51.62287095715006302, -23.73934037231757443, 11.05740245334329153 ) ) ;
#47206=CARTESIAN_POINT ( 'NONE',  ( -48.52287095715006870, -24.50216790748205042, 0.6166512839542480640 ) ) ;
#47207=CARTESIAN_POINT ( 'NONE',  ( -15.12424899162716230, 14.39509690008720177, -1.500000000000002220 ) ) ;
#47208=CARTESIAN_POINT ( 'NONE',  ( -21.69466673205137752, 2.402554924997643226, 11.49999999999999645 ) ) ;
#47210=CARTESIAN_POINT ( 'NONE',  ( -99.95716258256356923, -25.04656903514557698, 7.498856445056238051 ) ) ;
#47211=CARTESIAN_POINT ( 'NONE',  ( 6.846561153812083411, -21.39451737393737574, -1.500000000000002220 ) ) ;
#47212=CARTESIAN_POINT ( 'NONE',  ( -118.5174234704193310, -24.51419770103160189, 9.386484678747169852 ) ) ;
#47216=VERTEX_POINT ( 'NONE', #42219 ) ;
#47218=VERTEX_POINT ( 'NONE', #93735 ) ;
#47219=CARTESIAN_POINT ( 'NONE',  ( -15.06583839362908961, -15.15408912208086534, -1.500000000000002220 ) ) ;
#47220=CARTESIAN_POINT ( 'NONE',  ( -17.59303920844588376, -13.82112144285918731, 11.49999999999999645 ) ) ;
#47221=ORIENTED_EDGE ( 'NONE', *, *, #22650, .F. ) ;
#47222=CARTESIAN_POINT ( 'NONE',  ( -8.945158345017247825, -19.07159632999312393, -1.500000000000002220 ) ) ;
#47223=CARTESIAN_POINT ( 'NONE',  ( -103.6228709571500559, -29.50247984919015209, -1.443849546365050029 ) ) ;
#47224=CARTESIAN_POINT ( 'NONE',  ( -13.68957358570155769, -14.46295258127404892, -1.500000000000002220 ) ) ;
#47226=B_SPLINE_CURVE_WITH_KNOTS ( 'NONE', 3,
 ( #89224, #50664, #81612, #26821, #58773, #89725, #74489, #36426 ),
 .UNSPECIFIED., .F., .F.,
 ( 4, 2, 2, 4 ),
 ( -0.001240666984356068306, -0.0002401179793396698847, 0.0007604310256767281024, 0.002761529035709520824 ),
 .UNSPECIFIED. ) ;
#47227=CARTESIAN_POINT ( 'NONE',  ( -49.96215261998537471, -25.05234313451448713, 7.519799490366015249 ) ) ;
#47228=CARTESIAN_POINT ( 'NONE',  ( -15.01370250125036421, 16.05796621403891677, -1.500000000000002220 ) ) ;
#47231=DIRECTION ( 'NONE',  ( -3.773278334444166432E-23, 1.000000000000000000, 0.000000000000000000 ) ) ;
#47232=DIRECTION ( 'NONE',  ( 0.000000000000000000, -0.9999999999976377785, -2.173523156925979128E-06 ) ) ;
#47233=CARTESIAN_POINT ( 'NONE',  ( -17.17656601037699104, 11.78060583124977256, 11.49999999999999645 ) ) ;
#47234=CARTESIAN_POINT ( 'NONE',  ( -74.52287095715007581, -24.65952944569304606, 1.056160979905697239 ) ) ;
#47235=VECTOR ( 'NONE', #44268, 1000.000000000000114 ) ;
#47239=CARTESIAN_POINT ( 'NONE',  ( -10.68834330497911189, 18.46263264838738039, 11.49999999999998934 ) ) ;
#47241=CARTESIAN_POINT ( 'NONE',  ( -51.16008406385073926, -25.23528994651498891, 3.604084673499913904 ) ) ;
#47242=DIRECTION ( 'NONE',  ( 0.000000000000000000, 0.9999999999976377785, 2.173523156925979128E-06 ) ) ;
#47243=CARTESIAN_POINT ( 'NONE',  ( -69.33173068595476707, -25.22594453560301631, 6.517383687127669134 ) ) ;
#47244=CARTESIAN_POINT ( 'NONE',  ( 21.70358988458699301, 5.938112137899119070, -1.500000000000002220 ) ) ;
#47245=EDGE_CURVE ( 'NONE', #58299, #3436, #72737, .T. ) ;
#47246=FACE_OUTER_BOUND ( 'NONE', #52096, .T. ) ;
#47247=VERTEX_POINT ( 'NONE', #54694 ) ;
#47251=CARTESIAN_POINT ( 'NONE',  ( -17.62174901100306101, -8.731699659924187173, 11.49999999999999645 ) ) ;
#47255=ADVANCED_FACE ( 'NONE', ( #99346 ), #53248, .T. ) ;
#47257=CARTESIAN_POINT ( 'NONE',  ( -39.58953762381673158, -24.65952944569304606, 1.056160979905693686 ) ) ;
#47258=CARTESIAN_POINT ( 'NONE',  ( -100.4277023991755442, -25.25095780761413522, 5.215800478967231868 ) ) ;
#47260=EDGE_CURVE ( 'NONE', #58493, #71422, #7504, .T. ) ;
#47262=CARTESIAN_POINT ( 'NONE',  ( 3.553741186906278493, -19.43417129498564577, 11.49999999999998934 ) ) ;
#47263=VERTEX_POINT ( 'NONE', #45085 ) ;
#47264=EDGE_CURVE ( 'NONE', #12032, #59480, #21838, .T. ) ;
#47266=AXIS2_PLACEMENT_3D ( 'NONE', #88288, #3554, #11646 ) ;
#47268=EDGE_LOOP ( 'NONE', ( #86112, #61230, #87486, #40494 ) ) ;
#47274=CARTESIAN_POINT ( 'NONE',  ( -67.58953762381672448, -24.64965694238407323, 8.947790433994653014 ) ) ;
#47275=CARTESIAN_POINT ( 'NONE',  ( -107.6235340116869423, -24.65952944569304606, 1.056160979905704789 ) ) ;
#47276=CARTESIAN_POINT ( 'NONE',  ( 1.468936567494551593, -19.95401460376903913, 11.49999999999998934 ) ) ;
#47277=B_SPLINE_CURVE_WITH_KNOTS ( 'NONE', 3,
 ( #39011, #15676, #78558, #77561 ),
 .UNSPECIFIED., .F., .F.,
 ( 4, 4 ),
 ( 0.000000000000000000, 0.002085937500000023537 ),
 .UNSPECIFIED. ) ;
#47279=CARTESIAN_POINT ( 'NONE',  ( -99.77116551335946326, -25.10935072017632308, 2.990445978756222978 ) ) ;
#47280=CARTESIAN_POINT ( 'NONE',  ( -116.5876139491709154, -24.66019654487199730, 8.947790411086115725 ) ) ;
#47282=ADVANCED_FACE ( 'NONE', ( #100328 ), #31398, .T. ) ;
#47283=CARTESIAN_POINT ( 'NONE',  ( -79.58490835860241930, -24.51419770103157347, 9.386484678747176957 ) ) ;
#47284=CARTESIAN_POINT ( 'NONE',  ( -110.3009842343709721, -25.29012725628788516, 3.294836594238610417 ) ) ;
#47285=CARTESIAN_POINT ( 'NONE',  ( -65.62287095715005592, -29.50248789122583659, 2.256150453626215580 ) ) ;
#47288=FACE_OUTER_BOUND ( 'NONE', #20969, .T. ) ;
#47289=DIRECTION ( 'NONE',  ( 0.000000000000000000, 0.9999999999976377785, 2.173523156925979128E-06 ) ) ;
#47290=ADVANCED_FACE ( 'NONE', ( #71925 ), #86132, .T. ) ;
#47291=PLANE ( 'NONE',  #57667 ) ;
#47292=CARTESIAN_POINT ( 'NONE',  ( -36.52287095715006870, -24.64965694238407323, 8.947790433994205372 ) ) ;
#47294=CARTESIAN_POINT ( 'NONE',  ( -11.07518157712430096, -17.02944518001645946, 11.49999999999998934 ) ) ;
#47296=CARTESIAN_POINT ( 'NONE',  ( -88.58953762381671027, -23.48786465467241769, 11.44779295918254114 ) ) ;
#47298=EDGE_LOOP ( 'NONE', ( #43110, #66205, #90887, #94341 ) ) ;
#47299=DIRECTION ( 'NONE',  ( -1.000000000000000000, -3.773278334444167608E-23, -8.201307833595939069E-29 ) ) ;
#47301=CARTESIAN_POINT ( 'NONE',  ( 19.31759285448427477, -5.727529672960866236, -1.500000000000002220 ) ) ;
#47302=CARTESIAN_POINT ( 'NONE',  ( 17.87031378931267867, -11.31994873005049129, 11.49999999999999645 ) ) ;
#47304=CARTESIAN_POINT ( 'NONE',  ( 21.80885565983754404, 3.581153529568561478, -1.500000000000002220 ) ) ;
#47305=EDGE_CURVE ( 'NONE', #68548, #95766, #46137, .T. ) ;
#47306=CARTESIAN_POINT ( 'NONE',  ( -17.20787902393383462, -11.26661214947554157, 11.49999999999998934 ) ) ;
#47307=CARTESIAN_POINT ( 'NONE',  ( -60.62821588322990607, -24.83618233451449697, 1.606449574219536380 ) ) ;
#47308=ORIENTED_EDGE ( 'NONE', *, *, #1754, .F. ) ;
#47309=CARTESIAN_POINT ( 'NONE',  ( -88.52287095715006160, -23.47596703998600631, 11.44779298504228393 ) ) ;
#47312=CARTESIAN_POINT ( 'NONE',  ( -61.62287095715007013, -23.73934037231757088, 11.05740245334329330 ) ) ;
#47315=VERTEX_POINT ( 'NONE', #3419 ) ;
#47316=PLANE ( 'NONE',  #31057 ) ;
#47318=CARTESIAN_POINT ( 'NONE',  ( -68.49379447780960106, -24.66019654487199375, 8.947790411086122830 ) ) ;
#47319=CARTESIAN_POINT ( 'NONE',  ( 7.614520588612671226, -19.20288753073135268, -1.500000000000002220 ) ) ;
#47320=EDGE_CURVE ( 'NONE', #85117, #14223, #94740, .T. ) ;
#47321=B_SPLINE_CURVE_WITH_KNOTS ( 'NONE', 3,
 ( #67994, #76081, #45158, #14181 ),
 .UNSPECIFIED., .F., .F.,
 ( 4, 4 ),
 ( 0.000000000000000000, 9.999999999998897304E-05 ),
 .UNSPECIFIED. ) ;
#47322=CARTESIAN_POINT ( 'NONE',  ( -21.46818342838279392, -2.986162219498790904, 11.49999999999999645 ) ) ;
#47324=CARTESIAN_POINT ( 'NONE',  ( -37.62287095715005592, -29.50248528299804818, 1.056150453629031594 ) ) ;
#47326=CARTESIAN_POINT ( 'NONE',  ( -1.986123035288760885, 22.30159847666916662, 11.49999999999998934 ) ) ;
#47327=CARTESIAN_POINT ( 'NONE',  ( -47.57718451496743484, -24.66019654487199730, 8.947790411086117501 ) ) ;
#47328=CARTESIAN_POINT ( 'NONE',  ( -120.6228709571500417, -24.99156045073393528, 7.747789690856161648 ) ) ;
#47330=CARTESIAN_POINT ( 'NONE',  ( -116.7734038585102354, -25.37178273948851626, 5.922773836801656699 ) ) ;
#47331=CARTESIAN_POINT ( 'NONE',  ( -35.62710583289069177, -23.48786465467240703, 11.44779295918255180 ) ) ;
#47332=VERTEX_POINT ( 'NONE', #25734 ) ;
#47333=B_SPLINE_CURVE_WITH_KNOTS ( 'NONE', 3,
 ( #59895, #27931, #73611, #58398 ),
 .UNSPECIFIED., .F., .F.,
 ( 4, 4 ),
 ( 0.000000000000000000, 9.999999999998897304E-05 ),
 .UNSPECIFIED. ) ;
#47335=ORIENTED_EDGE ( 'NONE', *, *, #21830, .T. ) ;
#47337=CARTESIAN_POINT ( 'NONE',  ( -109.6260462722971454, -24.35071581493543746, 9.817618358456025263 ) ) ;
#47338=CARTESIAN_POINT ( 'NONE',  ( 20.71511372717374755, 4.256074106246791722, -1.500000000000002220 ) ) ;
#47339=ORIENTED_EDGE ( 'NONE', *, *, #40743, .T. ) ;
#47340=CARTESIAN_POINT ( 'NONE',  ( -50.56030698869226114, -23.85016227208580020, -0.8807180028928345283 ) ) ;
#47341=CARTESIAN_POINT ( 'NONE',  ( -20.57666286913221754, 7.287794730890116313, -1.500000000000002220 ) ) ;
#47342=CARTESIAN_POINT ( 'NONE',  ( -38.52287095715006870, -23.47596703998600631, 11.44779298504229281 ) ) ;
#47345=CARTESIAN_POINT ( 'NONE',  ( -12.45635911906152771, -17.91357634596933934, -1.500000000000002220 ) ) ;
#47348=DIRECTION ( 'NONE',  ( 0.000000000000000000, -0.9999999999976377785, -2.173523156925979128E-06 ) ) ;
#47349=CARTESIAN_POINT ( 'NONE',  ( -85.63839554153061329, -24.15602025860895807, 10.28564288303535967 ) ) ;
#47352=ORIENTED_EDGE ( 'NONE', *, *, #77012, .F. ) ;
#47353=AXIS2_PLACEMENT_3D ( 'NONE', #29660, #74832, #51018 ) ;
#47354=CARTESIAN_POINT ( 'NONE',  ( -58.62287095715004881, -24.64965695001468404, 8.947790433994185832 ) ) ;
#47356=CARTESIAN_POINT ( 'NONE',  ( -6.410030533929251817, 20.24415959294862333, -1.500000000000002220 ) ) ;
#47358=CARTESIAN_POINT ( 'NONE',  ( -94.50778353013456012, -24.51314013834316086, 0.6176544820404165081 ) ) ;
#47359=CARTESIAN_POINT ( 'NONE',  ( -79.14729083585920932, -25.27791806053743073, 6.795304352983273510 ) ) ;
#47360=DIRECTION ( 'NONE',  ( -3.773278334453079030E-23, 0.9999999999976377785, 2.173523156925979128E-06 ) ) ;
#47361=DIRECTION ( 'NONE',  ( -3.773278334453079030E-23, 0.9999999999976377785, 2.173523156925979128E-06 ) ) ;
#47362=CARTESIAN_POINT ( 'NONE',  ( 8.665315094346039970, 17.34094453737590769, 11.49999999999998934 ) ) ;
#47364=CARTESIAN_POINT ( 'NONE',  ( -39.02714944717881451, -25.25978494880519776, 3.590542803917028181 ) ) ;
#47365=ORIENTED_EDGE ( 'NONE', *, *, #84579, .T. ) ;
#47366=EDGE_CURVE ( 'NONE', #86594, #38515, #81176, .T. ) ;
#47367=CARTESIAN_POINT ( 'NONE',  ( -17.64752530894654470, 8.349842952099315596, 11.49999999999999645 ) ) ;
#47369=EDGE_CURVE ( 'NONE', #96261, #59330, #40019, .T. ) ;
#47370=CARTESIAN_POINT ( 'NONE',  ( -91.94687923781920347, -29.50249691823240994, 6.409318347766594037 ) ) ;
#47372=EDGE_CURVE ( 'NONE', #53534, #17650, #73993, .T. ) ;
#47373=CARTESIAN_POINT ( 'NONE',  ( -98.55620429048339304, -24.66019654487199730, 8.947790411086124607 ) ) ;
#47376=CARTESIAN_POINT ( 'NONE',  ( -106.5228709571500332, -23.94994826722564696, -0.6494450866342710293 ) ) ;
#47378=CARTESIAN_POINT ( 'NONE',  ( -34.58953762381672448, -23.48786465467240347, 11.44779295918255535 ) ) ;
#47379=CARTESIAN_POINT ( 'NONE',  ( 16.91694316922610497, -9.995573847407506207, -1.500000000000002220 ) ) ;
#47383=CARTESIAN_POINT ( 'NONE',  ( 21.36531308999010648, 3.172564587314818052, 11.49999999999998934 ) ) ;
#47384=CARTESIAN_POINT ( 'NONE',  ( -40.52987890412448024, -24.73486907724917927, 1.287355809206960577 ) ) ;
#47386=CARTESIAN_POINT ( 'NONE',  ( -23.05830607064937965, -0.9945063503333604338, -1.500000000000002220 ) ) ;
#47388=CARTESIAN_POINT ( 'NONE',  ( -121.6228709571500417, -29.50247984919015209, -1.443849546365046699 ) ) ;
#47389=CARTESIAN_POINT ( 'NONE',  ( -90.52287095715006160, -24.91570333825770334, 8.075032458260366752 ) ) ;
#47390=CARTESIAN_POINT ( 'NONE',  ( -121.5543276637445018, -24.35071581493543746, 9.817618358456025263 ) ) ;
#47391=DIRECTION ( 'NONE',  ( -0.000000000000000000, 2.173523156925979552E-06, -0.9999999999976378895 ) ) ;
#47392=CARTESIAN_POINT ( 'NONE',  ( -111.7814946224345789, -25.29824137189153532, 4.332404408885398794 ) ) ;
#47393=CARTESIAN_POINT ( 'NONE',  ( -129.5558065563047876, -24.34968618360934300, 0.1864209137778921610 ) ) ;
#47394=VECTOR ( 'NONE', #10892, 1000.000000000000114 ) ;
#47395=B_SPLINE_CURVE_WITH_KNOTS ( 'NONE', 3,
 ( #34705, #36202, #66178, #5244 ),
 .UNSPECIFIED., .F., .F.,
 ( 4, 4 ),
 ( 0.3390065795743660848, 0.3400073266151316109 ),
 .UNSPECIFIED. ) ;
#47396=CARTESIAN_POINT ( 'NONE',  ( -49.58953762381673158, -23.47593901973091235, -1.443836447539009749 ) ) ;
#47397=CARTESIAN_POINT ( 'NONE',  ( -16.79965634883036074, 10.71410036745690597, -1.500000000000002220 ) ) ;
#47399=CARTESIAN_POINT ( 'NONE',  ( 13.99221305778824487, -14.08248706038611964, -1.500000000000002220 ) ) ;
#47402=CARTESIAN_POINT ( 'NONE',  ( -35.62287095715006302, -24.51254535404254398, 9.355368623467647637 ) ) ;
#47403=CARTESIAN_POINT ( 'NONE',  ( -3.546427018491999483, -20.45703643143680850, 11.49999999999999645 ) ) ;
#47404=LINE ( 'NONE', #63139, #67849 ) ;
#47405=CARTESIAN_POINT ( 'NONE',  ( -106.5112401517874190, -24.65952944569304961, 1.056160979905703456 ) ) ;
#47406=CARTESIAN_POINT ( 'NONE',  ( -21.69093436787670726, -6.948586514802197023, 11.49999999999999645 ) ) ;
#47408=ORIENTED_EDGE ( 'NONE', *, *, #89855, .T. ) ;
#47409=B_SPLINE_SURFACE_WITH_KNOTS ( 'NONE', 3, 1, ( 
 ( #72814, #65716 ),
 ( #89032, #4296 ),
 ( #49986, #26634 ),
 ( #74299, #90025 ),
 ( #81912, #81417 ),
 ( #43363, #34248 ),
 ( #80913, #20497 ),
 ( #74784, #28131 ),
 ( #3317, #50975 ),
 ( #10907, #65223 ),
 ( #4791, #96629 ),
 ( #96147, #57098 ),
 ( #80413, #88035 ),
 ( #27132, #42867 ),
 ( #27636, #11404 ) ),
 .UNSPECIFIED., .F., .F., .F.,
 ( 4, 1, 1, 1, 1, 1, 1, 1, 1, 1, 1, 1, 4 ),
 ( 2, 2 ),
 ( 0.000000000000000000, 0.09468725186755398704, 0.1819941557072748128, 0.2643769486105100874, 0.3421798619477735559, 0.4186176108621474934, 0.4965090753719113015, 0.5773690916117304450, 0.6615105924541956339, 0.7467325508291923208, 0.8312579843277431157, 0.9152056162136544826, 1.000000000000000000 ),
 ( 0.000000000000000000, 1.000000000000000000 ),
 .UNSPECIFIED. ) ;
#47410=CARTESIAN_POINT ( 'NONE',  ( -83.62287095715007013, -24.66019654487199730, 8.947790411086126383 ) ) ;
#47411=CARTESIAN_POINT ( 'NONE',  ( -106.6228709571500559, -23.47593901973091235, -1.443836447538999312 ) ) ;
#47412=ORIENTED_EDGE ( 'NONE', *, *, #24395, .T. ) ;
#47413=B_SPLINE_CURVE_WITH_KNOTS ( 'NONE', 3,
 ( #74119, #11706, #20309, #35062, #90336, #58896 ),
 .UNSPECIFIED., .F., .F.,
 ( 4, 2, 4 ),
 ( 0.000000000000000000, 0.001380764517854769519, 0.002761529035709539039 ),
 .UNSPECIFIED. ) ;
#47414=CARTESIAN_POINT ( 'NONE',  ( -16.64171244834553676, 11.49637152377623828, 11.49999999999998934 ) ) ;
#47415=CARTESIAN_POINT ( 'NONE',  ( -77.52287095715006160, -23.48786465467241058, 11.44779295918254469 ) ) ;
#47416=CARTESIAN_POINT ( 'NONE',  ( -97.62287095714999907, -24.33927499327854704, 9.819080762295818943 ) ) ;
#47418=CARTESIAN_POINT ( 'NONE',  ( -70.62287095715004170, -24.14406661707768009, 10.28769366152058673 ) ) ;
#47419=CARTESIAN_POINT ( 'NONE',  ( -22.88579126497628025, -1.409509213828211927, 11.49999999999998934 ) ) ;
#47420=CARTESIAN_POINT ( 'NONE',  ( -40.80373042471702405, -25.12778184171447649, 2.872918476217471540 ) ) ;
#47421=CARTESIAN_POINT ( 'NONE',  ( -4.285004571687458963, -21.18589511591401831, -1.500000000000002220 ) ) ;
#47422=DIRECTION ( 'NONE',  ( 3.773278334444166432E-23, -1.000000000000000000, 0.000000000000000000 ) ) ;
#47423=AXIS2_PLACEMENT_3D ( 'NONE', #32778, #63758, #47009 ) ;
#47424=CARTESIAN_POINT ( 'NONE',  ( -2.499008156623981236, -20.81284420272260860, 11.49999999999999645 ) ) ;
#47426=CARTESIAN_POINT ( 'NONE',  ( -73.58953762381672448, -23.48786465467241058, 11.44779295918254469 ) ) ;
#47427=CARTESIAN_POINT ( 'NONE',  ( -69.23586867255411903, -25.31612525200183228, 5.333582893051659113 ) ) ;
#47428=CARTESIAN_POINT ( 'NONE',  ( 4.628415685485613551, -21.52068878818806752, -1.500000000000002220 ) ) ;
#47429=EDGE_CURVE ( 'NONE', #1915, #26773, #60707, .T. ) ;
#47432=CARTESIAN_POINT ( 'NONE',  ( -49.86550021440504565, -25.27344785826827689, 3.414711230909520001 ) ) ;
#47433=ADVANCED_FACE ( 'NONE', ( #89633 ), #81025, .F. ) ;
#47434=CARTESIAN_POINT ( 'NONE',  ( -122.6228709571500417, -24.64965695001469115, 8.947790433994175174 ) ) ;
#47436=CARTESIAN_POINT ( 'NONE',  ( -86.62287095715004170, -29.50248528299804818, 1.056150453629040253 ) ) ;
#47437=VERTEX_POINT ( 'NONE', #12993 ) ;
#47440=CARTESIAN_POINT ( 'NONE',  ( -71.62287095715005592, -23.47596703998600631, 11.44779298504227683 ) ) ;
#47442=CARTESIAN_POINT ( 'NONE',  ( -19.82921842031888104, 5.099586017421429140, -1.500000000000002220 ) ) ;
#47443=ORIENTED_EDGE ( 'NONE', *, *, #90736, .T. ) ;
#47444=CARTESIAN_POINT ( 'NONE',  ( -99.30054463691881494, -25.25874007465087701, 6.071601063123229558 ) ) ;
#47445=CARTESIAN_POINT ( 'NONE',  ( -44.65451812762749739, -23.73766607897669800, -1.055555164236458898 ) ) ;
#47447=CARTESIAN_POINT ( 'NONE',  ( -3.941980378682776287, 21.93750326593198352, 11.49999999999998934 ) ) ;
#47448=VECTOR ( 'NONE', #50999, 1000.000000000000114 ) ;
#47449=CARTESIAN_POINT ( 'NONE',  ( -70.32380231474228083, -25.13313949306887096, 7.101635536975467566 ) ) ;
#47450=FACE_OUTER_BOUND ( 'NONE', #38130, .T. ) ;
#47451=ORIENTED_EDGE ( 'NONE', *, *, #29663, .T. ) ;
#47452=CARTESIAN_POINT ( 'NONE',  ( -29.68686754081408807, -25.14195210743483955, 3.478271856783234917 ) ) ;
#47455=CARTESIAN_POINT ( 'NONE',  ( -19.40898059523135544, 7.551958013340856368, -1.500000000000002220 ) ) ;
#47457=DIRECTION ( 'NONE',  ( 3.773278334444167608E-23, -1.000000000000000000, 0.000000000000000000 ) ) ;
#47459=VERTEX_POINT ( 'NONE', #44465 ) ;
#47460=AXIS2_PLACEMENT_3D ( 'NONE', #28406, #13176, #14175 ) ;
#47461=CARTESIAN_POINT ( 'NONE',  ( -50.71600500446225368, -25.25854563549779641, 7.074608752973259307 ) ) ;
#47462=CARTESIAN_POINT ( 'NONE',  ( -18.19455084753484542, -10.52586660885228298, -1.500000000000002220 ) ) ;
#47464=CARTESIAN_POINT ( 'NONE',  ( -118.5228709571500900, -23.72773821059536914, 11.05748984161097326 ) ) ;
#47467=AXIS2_PLACEMENT_3D ( 'NONE', #97249, #27741, #52079 ) ;
#47468=CARTESIAN_POINT ( 'NONE',  ( -86.62359152838003240, -24.66019654487200086, 8.947790411086115725 ) ) ;
#47469=CARTESIAN_POINT ( 'NONE',  ( -60.62287095715004881, -23.47596703998600631, 11.44779298504227505 ) ) ;
#47470=CARTESIAN_POINT ( 'NONE',  ( -65.62287095714999907, -24.63345952396255356, 9.038047939301506517 ) ) ;
#47471=CARTESIAN_POINT ( 'NONE',  ( 4.265775719338400052, 21.77767432286298543, 11.49999999999999645 ) ) ;
#47473=CARTESIAN_POINT ( 'NONE',  ( -89.06226385320383088, -25.26877915520014994, 5.947789088310639904 ) ) ;
#47475=ORIENTED_EDGE ( 'NONE', *, *, #10843, .T. ) ;
#47476=CARTESIAN_POINT ( 'NONE',  ( -19.66899025692886838, 11.29834648773183581, 11.49999999999998934 ) ) ;
#47477=EDGE_CURVE ( 'NONE', #69684, #37312, #27975, .T. ) ;
#47479=ORIENTED_EDGE ( 'NONE', *, *, #72374, .T. ) ;
#47480=VERTEX_POINT ( 'NONE', #97245 ) ;
#47481=CARTESIAN_POINT ( 'NONE',  ( -68.52287095715006160, -23.47596703998600631, 11.44779298504228748 ) ) ;
#47482=CARTESIAN_POINT ( 'NONE',  ( -11.96439459519798554, -16.23097265130270728, 11.49999999999998934 ) ) ;
#47487=CARTESIAN_POINT ( 'NONE',  ( 19.55810785529653373, 10.91776788121007868, -1.500000000000002220 ) ) ;
#47488=ORIENTED_EDGE ( 'NONE', *, *, #63658, .F. ) ;
#47489=ORIENTED_EDGE ( 'NONE', *, *, #36830, .T. ) ;
#47490=CARTESIAN_POINT ( 'NONE',  ( -30.64751926837171325, -23.47596703998600631, 11.44779298504228038 ) ) ;
#47492=FACE_OUTER_BOUND ( 'NONE', #46185, .T. ) ;
#47493=EDGE_CURVE ( 'NONE', #12728, #45608, #67884, .T. ) ;
#47494=PLANE ( 'NONE',  #99218 ) ;
#47496=EDGE_CURVE ( 'NONE', #3648, #58574, #12153, .T. ) ;
#47497=FACE_BOUND ( 'NONE', #21853, .T. ) ;
#47498=CARTESIAN_POINT ( 'NONE',  ( -10.82925958622295859, 16.30987832687952022, 11.49999999999998934 ) ) ;
#47500=EDGE_CURVE ( 'NONE', #64821, #30992, #111, .T. ) ;
#47501=CARTESIAN_POINT ( 'NONE',  ( -52.52287095715006870, -23.47596703998600631, 11.44779298504229104 ) ) ;
#47503=CARTESIAN_POINT ( 'NONE',  ( -2.374466145016132845, -21.38244973876172494, -1.500000000000002220 ) ) ;
#47505=ADVANCED_FACE ( 'NONE', ( #21104 ), #57698, .F. ) ;
#47506=CARTESIAN_POINT ( 'NONE',  ( -121.5228709571500616, -24.65952944569305316, 1.056160979905705899 ) ) ;
#47508=CARTESIAN_POINT ( 'NONE',  ( -68.62287095715007013, -24.33927499327854704, 9.819080762295815390 ) ) ;
#47509=CARTESIAN_POINT ( 'NONE',  ( 22.85676281555306844, 1.471244944367766649, -1.500000000000002220 ) ) ;
#47510=B_SPLINE_CURVE_WITH_KNOTS ( 'NONE', 3,
 ( #65077, #95994, #94488, #73658 ),
 .UNSPECIFIED., .F., .F.,
 ( 4, 4 ),
 ( 0.000000000000000000, 0.0001002978982766898939 ),
 .UNSPECIFIED. ) ;
#47512=CARTESIAN_POINT ( 'NONE',  ( -124.5562042904833504, -24.64965694238575367, 8.947790433994187609 ) ) ;
#47513=CARTESIAN_POINT ( 'NONE',  ( -71.11503856163616888, -25.29900863253169518, 5.642877111387134548 ) ) ;
#47514=CARTESIAN_POINT ( 'NONE',  ( 19.65109224456760728, -3.968444974485820786, 11.49999999999999645 ) ) ;
#47515=CARTESIAN_POINT ( 'NONE',  ( -79.44434589896187049, -25.26612442218368670, 4.820847248093164339 ) ) ;
#47516=CARTESIAN_POINT ( 'NONE',  ( -57.58953762381671737, -24.66019654487199020, 8.947790411086133489 ) ) ;
#47519=ORIENTED_EDGE ( 'NONE', *, *, #16038, .T. ) ;
#47520=EDGE_CURVE ( 'NONE', #50701, #48998, #90867, .T. ) ;
#47521=FACE_OUTER_BOUND ( 'NONE', #25288, .T. ) ;
#47522=CARTESIAN_POINT ( 'NONE',  ( 15.29254711327534899, -15.47666941828629739, 11.49999999999998934 ) ) ;
#47523=CARTESIAN_POINT ( 'NONE',  ( -45.52287095715007581, -24.15516710230293995, 10.28746687063727272 ) ) ;
#47524=CARTESIAN_POINT ( 'NONE',  ( 18.70796670040472165, 5.986831462552164140, -1.500000000000002220 ) ) ;
#47525=CARTESIAN_POINT ( 'NONE',  ( -34.52287095715006160, -23.47593901973090169, -1.443836447538997314 ) ) ;
#47527=CARTESIAN_POINT ( 'NONE',  ( -109.5056412146432052, -25.31698062991398501, 4.749485475450724969 ) ) ;
#47530=CARTESIAN_POINT ( 'NONE',  ( -62.52287095715003318, -24.66019654487199730, 8.947790411086124607 ) ) ;
#47531=LINE ( 'NONE', #1853, #553 ) ;
#47532=CARTESIAN_POINT ( 'NONE',  ( 7.805751503010069037, -19.01748540344778959, 11.49999999999999645 ) ) ;
#47534=CARTESIAN_POINT ( 'NONE',  ( -120.5936529139786160, -23.48783264082477018, -1.443836473390085695 ) ) ;
#47535=AXIS2_PLACEMENT_3D ( 'NONE', #34176, #65148, #33163 ) ;
#47536=CARTESIAN_POINT ( 'NONE',  ( 22.24477432615492134, 4.004077059304647968, 11.49999999999999645 ) ) ;
#47537=VERTEX_POINT ( 'NONE', #81529 ) ;
#47538=CARTESIAN_POINT ( 'NONE',  ( -99.72794805030189025, -25.31296386855978753, 4.442265286386216872 ) ) ;
#47541=DIRECTION ( 'NONE',  ( 0.000000000000000000, -0.9999999999976377785, -2.173523156925979128E-06 ) ) ;
#47542=AXIS2_PLACEMENT_3D ( 'NONE', #80308, #26527, #18900 ) ;
#47544=CARTESIAN_POINT ( 'NONE',  ( -25.63919700385670453, -24.93063196310097496, 6.233789962485477787 ) ) ;
#47545=DIRECTION ( 'NONE',  ( 0.8253571461740011328, -1.227195083036775770E-06, 0.5646109999442116001 ) ) ;
#47546=EDGE_CURVE ( 'NONE', #33967, #81135, #64314, .T. ) ;
#47548=CARTESIAN_POINT ( 'NONE',  ( -79.98791220707269645, -25.26749890627193906, 5.033164624709036694 ) ) ;
#47549=CARTESIAN_POINT ( 'NONE',  ( 19.70479270790718829, 11.56945388388114360, 11.49999999999998934 ) ) ;
#47551=B_SPLINE_SURFACE_WITH_KNOTS ( 'NONE', 3, 1, ( 
 ( #27167, #34779 ),
 ( #58128, #89560 ),
 ( #50501, #10940 ),
 ( #51008, #3347 ),
 ( #74334, #25658 ),
 ( #56631, #11933 ),
 ( #64759, #42898 ),
 ( #87560, #26159 ),
 ( #73344, #88068 ),
 ( #35285, #49514 ),
 ( #96181, #57626 ),
 ( #3837, #88567 ),
 ( #91545, #67237 ),
 ( #23908, #13918 ),
 ( #20530, #83429 ),
 ( #98652, #51505 ),
 ( #82437, #5315 ),
 ( #51999, #77680 ),
 ( #67737, #74821 ) ),
 .UNSPECIFIED., .F., .F., .F.,
 ( 4, 1, 1, 1, 1, 1, 1, 1, 1, 1, 1, 1, 1, 1, 1, 1, 4 ),
 ( 2, 2 ),
 ( 0.000000000000000000, 0.06184170298390887638, 0.1212623730944471651, 0.1807459488653155588, 0.2392309018221052130, 0.2983075587884627122, 0.3581827976158459825, 0.4203592307800690930, 0.4847924155141860592, 0.5499384837666880799, 0.6137182775404268487, 0.6766807072496276998, 0.7391541704483146624, 0.8021997032403502814, 0.8667401776162937388, 0.9320496524002453986, 1.000000000000000000 ),
 ( 0.000000000000000000, 1.000000000000000000 ),
 .UNSPECIFIED. ) ;
#47552=CARTESIAN_POINT ( 'NONE',  ( -96.59125222054736071, -24.15543982623907482, -0.2315651400026596807 ) ) ;
#47553=DIRECTION ( 'NONE',  ( 0.000000000000000000, 0.9999999999976377785, 2.173523156925979128E-06 ) ) ;
#47554=CARTESIAN_POINT ( 'NONE',  ( 0.2029947971921062799, -22.41465419638480228, 11.49999999999999645 ) ) ;
#47555=ORIENTED_EDGE ( 'NONE', *, *, #29938, .T. ) ;
#47556=B_SPLINE_CURVE_WITH_KNOTS ( 'NONE', 3,
 ( #39815, #70773, #16975, #9867 ),
 .UNSPECIFIED., .F., .F.,
 ( 4, 4 ),
 ( 0.000000000000000000, 0.0004038461538461574074 ),
 .UNSPECIFIED. ) ;
#47557=FACE_OUTER_BOUND ( 'NONE', #42326, .T. ) ;
#47558=CARTESIAN_POINT ( 'NONE',  ( 5.197331492371871420, 21.31670716312865466, -1.500000000000002220 ) ) ;
#47559=ADVANCED_FACE ( 'NONE', ( #35357 ), #90458, .T. ) ;
#47560=DIRECTION ( 'NONE',  ( -3.773278334444167020E-23, 1.000000000000000000, 0.000000000000000000 ) ) ;
#47561=CARTESIAN_POINT ( 'NONE',  ( -34.58065475290599267, -24.51419770103156637, 9.386484678747176957 ) ) ;
#47563=VERTEX_POINT ( 'NONE', #53078 ) ;
#47564=CARTESIAN_POINT ( 'NONE',  ( -48.64595118538275642, -23.96169478059712787, 10.65365249895718236 ) ) ;
#47565=EDGE_CURVE ( 'NONE', #79650, #100062, #31556, .T. ) ;
#47568=CARTESIAN_POINT ( 'NONE',  ( -7.951223608505463503, 18.87544906973805325, -1.500000000000002220 ) ) ;
#47570=ORIENTED_EDGE ( 'NONE', *, *, #63923, .F. ) ;
#47571=ORIENTED_EDGE ( 'NONE', *, *, #40565, .F. ) ;
#47573=CARTESIAN_POINT ( 'NONE',  ( -14.58522200957802184, -17.87834940746265389, -1.500000000000002220 ) ) ;
#47574=CARTESIAN_POINT ( 'NONE',  ( -82.52287095715006160, -23.47593901973090169, -1.443836447538996648 ) ) ;
#47575=CARTESIAN_POINT ( 'NONE',  ( -18.23349369547262810, -8.965252873808195133, -1.500000000000002220 ) ) ;
#47579=CARTESIAN_POINT ( 'NONE',  ( -37.55620429048340014, -23.48783264082478084, -1.443836473390071484 ) ) ;
#47580=DIRECTION ( 'NONE',  ( -3.773278334453080206E-23, 0.9999999999976377785, 2.173523156925979975E-06 ) ) ;
#47582=CARTESIAN_POINT ( 'NONE',  ( -4.253298834618286506, 21.06115358058179154, 11.49999999999999645 ) ) ;
#47583=ORIENTED_EDGE ( 'NONE', *, *, #56837, .T. ) ;
#47584=CARTESIAN_POINT ( 'NONE',  ( -79.58953762381672448, -24.66019654487198665, 8.947790411086133489 ) ) ;
#47585=CARTESIAN_POINT ( 'NONE',  ( -49.35320922236618912, -25.26385781559679344, 4.652611292282501587 ) ) ;
#47588=CARTESIAN_POINT ( 'NONE',  ( 18.78520451414993531, -8.817701518030307994, -1.500000000000002220 ) ) ;
#47589=ORIENTED_EDGE ( 'NONE', *, *, #51547, .F. ) ;
#47591=CARTESIAN_POINT ( 'NONE',  ( -125.5896781930176189, -24.52300882791529801, 0.6510814631126508045 ) ) ;
#47593=CARTESIAN_POINT ( 'NONE',  ( -41.65561799070277260, -23.73791477778911485, 11.05961554403170943 ) ) ;
#47594=CARTESIAN_POINT ( 'NONE',  ( -124.4728709571500360, -25.40558663563427189, 5.000950442582704270 ) ) ;
#47596=EDGE_LOOP ( 'NONE', ( #69652, #53891, #65164, #81424 ) ) ;
#47597=CARTESIAN_POINT ( 'NONE',  ( -109.5562042904834072, -23.47596703998600631, 11.44779298504227683 ) ) ;
#47598=CARTESIAN_POINT ( 'NONE',  ( -42.51345785107305630, -23.73791477778911485, 11.05961554403171299 ) ) ;
#47599=CARTESIAN_POINT ( 'NONE',  ( -43.62863212119529521, -24.51419770103157347, 9.386484678747178734 ) ) ;
#47600=CARTESIAN_POINT ( 'NONE',  ( -21.12052157030387889, 6.262089831203976331, 11.49999999999999645 ) ) ;
#47601=CARTESIAN_POINT ( 'NONE',  ( -89.59466469485998630, -23.96169478059713498, 10.65365249895717703 ) ) ;
#47602=CARTESIAN_POINT ( 'NONE',  ( -19.71520456405594857, 11.01310763156902972, 11.49999999999998934 ) ) ;
#47603=CARTESIAN_POINT ( 'NONE',  ( 8.398332666215036824, -19.25654272332048578, -1.500000000000002220 ) ) ;
#47605=DIRECTION ( 'NONE',  ( 0.000000000000000000, 2.173523156925980399E-06, -0.9999999999976378895 ) ) ;
#47607=VERTEX_POINT ( 'NONE', #45961 ) ;
#47608=PLANE ( 'NONE',  #41800 ) ;
#47609=AXIS2_PLACEMENT_3D ( 'NONE', #90804, #21769, #52743 ) ;
#47610=CARTESIAN_POINT ( 'NONE',  ( -113.6228709571500701, -24.33927499327855415, 9.819080762295810061 ) ) ;
#47612=CARTESIAN_POINT ( 'NONE',  ( 13.25904570721172604, 16.46799385432867169, -1.500000000000002220 ) ) ;
#47613=FACE_OUTER_BOUND ( 'NONE', #74899, .T. ) ;
#47614=CARTESIAN_POINT ( 'NONE',  ( -50.58702570880215177, -25.26041116158741318, 7.558808615179929191 ) ) ;
#47617=CARTESIAN_POINT ( 'NONE',  ( -77.52287095715006160, -29.50247984919015209, -1.443849546365053582 ) ) ;
#47618=CARTESIAN_POINT ( 'NONE',  ( -22.22723998432330106, 0.1330083165726352878, -1.500000000000002220 ) ) ;
#47620=B_SPLINE_CURVE_WITH_KNOTS ( 'NONE', 3,
 ( #38533, #31424, #62381, #54776, #77082, #85712 ),
 .UNSPECIFIED., .F., .F.,
 ( 4, 2, 4 ),
 ( 0.000000000000000000, 0.001380764517854766267, 0.002761529035709532533 ),
 .UNSPECIFIED. ) ;
#47621=CARTESIAN_POINT ( 'NONE',  ( -49.21454750704995007, -25.03220799397881891, 7.069183833275417328 ) ) ;
#47622=EDGE_CURVE ( 'NONE', #72609, #33400, #59427, .T. ) ;
#47623=EDGE_LOOP ( 'NONE', ( #3254, #61550, #29256, #85627 ) ) ;
#47624=CARTESIAN_POINT ( 'NONE',  ( -51.08169923747086472, -25.31633088894497519, 4.960537870539334371 ) ) ;
#47625=CARTESIAN_POINT ( 'NONE',  ( -64.62287095715004170, -24.33927499327854704, 9.819080762295820719 ) ) ;
#47626=CARTESIAN_POINT ( 'NONE',  ( -126.5209009042890784, -24.34968618360934300, 0.1864209137778884418 ) ) ;
#47627=CARTESIAN_POINT ( 'NONE',  ( -100.5075858015768517, -24.73486907724917927, 1.287355809206965240 ) ) ;
#47628=CARTESIAN_POINT ( 'NONE',  ( -61.52287095715007581, -23.47593901973090169, -1.443836447538997092 ) ) ;
#47629=CARTESIAN_POINT ( 'NONE',  ( -14.34788840963776124, 13.16932220997287928, 11.49999999999998934 ) ) ;
#47631=CARTESIAN_POINT ( 'NONE',  ( 19.34736296927903254, -9.154118057783460216, 11.49999999999998934 ) ) ;
#47632=CARTESIAN_POINT ( 'NONE',  ( -85.52287095715004739, -24.91570333825475103, 8.075032458260896107 ) ) ;
#47633=CARTESIAN_POINT ( 'NONE',  ( -60.53048506470604195, -24.92592662360294042, 8.075495902990192931 ) ) ;
#47634=ADVANCED_FACE ( 'NONE', ( #15982 ), #46954, .F. ) ;
#47635=CARTESIAN_POINT ( 'NONE',  ( -100.6228709571500559, -24.52323809116984421, 9.355190652339416602 ) ) ;
#47636=CARTESIAN_POINT ( 'NONE',  ( -101.3738023147422780, -25.27360125068057428, 3.986250616286608928 ) ) ;
#47637=CARTESIAN_POINT ( 'NONE',  ( 21.16149768242404861, -8.233860041645145955, -1.500000000000002220 ) ) ;
#47639=CARTESIAN_POINT ( 'NONE',  ( -80.52287095715007581, -24.82558206586144323, 1.605769216559446377 ) ) ;
#47640=CARTESIAN_POINT ( 'NONE',  ( -7.754168067426306266, 18.25094163199162622, 11.49999999999999645 ) ) ;
#47641=CARTESIAN_POINT ( 'NONE',  ( -123.5204172166400696, -24.15620529776629510, 10.23563542870659404 ) ) ;
#47642=CARTESIAN_POINT ( 'NONE',  ( -104.5228709571500758, -24.65952944569305316, 1.056160979905702346 ) ) ;
#47645=EDGE_CURVE ( 'NONE', #6118, #70435, #66639, .T. ) ;
#47648=AXIS2_PLACEMENT_3D ( 'NONE', #36435, #82114, #90227 ) ;
#47649=CARTESIAN_POINT ( 'NONE',  ( -51.43440959051734751, -25.27412327365844646, 3.290885351747372844 ) ) ;
#47650=CARTESIAN_POINT ( 'NONE',  ( -2.787017431591729988, -21.48445716988565835, -1.500000000000002220 ) ) ;
#47651=CARTESIAN_POINT ( 'NONE',  ( -29.62287095715004881, -24.57400415421967566, 8.947790463233827651 ) ) ;
#47652=CARTESIAN_POINT ( 'NONE',  ( -4.672984603565591755, -18.88948546680484242, -1.500000000000002220 ) ) ;
#47654=ORIENTED_EDGE ( 'NONE', *, *, #75381, .T. ) ;
#47656=CARTESIAN_POINT ( 'NONE',  ( 2.178911383790714584, -20.24183328246387958, 11.49999999999999645 ) ) ;
#47657=CARTESIAN_POINT ( 'NONE',  ( -110.5895376238167245, -23.48783264082479505, -1.443836473390060160 ) ) ;
#47658=CARTESIAN_POINT ( 'NONE',  ( -48.62287095715004881, -24.66019654487199020, 8.947790411086135265 ) ) ;
#47659=VERTEX_POINT ( 'NONE', #79888 ) ;
#47660=CARTESIAN_POINT ( 'NONE',  ( -28.52287095715005805, -29.50247984919081290, -1.443849243165460372 ) ) ;
#47662=CARTESIAN_POINT ( 'NONE',  ( -39.31539998891226162, -25.27985467206300640, 5.139621229108158218 ) ) ;
#47663=CARTESIAN_POINT ( 'NONE',  ( -40.52633280619024703, -24.83644354573577928, 8.397322867130096569 ) ) ;
#47664=FACE_OUTER_BOUND ( 'NONE', #5062, .T. ) ;
#47665=CARTESIAN_POINT ( 'NONE',  ( 15.80722972286721983, -12.41807379269815215, -1.500000000000002220 ) ) ;
#47667=DIRECTION ( 'NONE',  ( -1.000000000000000000, -3.773278334444167608E-23, -8.201307833595939069E-29 ) ) ;
#47669=CARTESIAN_POINT ( 'NONE',  ( -66.51586011922388764, -23.73791477778911840, 11.05961554403170766 ) ) ;
#47671=CARTESIAN_POINT ( 'NONE',  ( 17.43399715339889511, -14.94103553264482720, 11.49999999999999645 ) ) ;
#47672=CARTESIAN_POINT ( 'NONE',  ( -9.076218414377828836, -20.82814578352222767, 11.49999999999998934 ) ) ;
#47673=EDGE_LOOP ( 'NONE', ( #78667, #56316, #8128, #25876 ) ) ;
#47674=CARTESIAN_POINT ( 'NONE',  ( -30.47287095715005734, -23.78331967171602201, 10.94926139022358669 ) ) ;
#47677=CARTESIAN_POINT ( 'NONE',  ( -105.5228709571501042, -23.48783264082477018, -1.443836473390085917 ) ) ;
#47678=EDGE_CURVE ( 'NONE', #55816, #91672, #48477, .T. ) ;
#47679=CARTESIAN_POINT ( 'NONE',  ( -128.5554931858794703, -24.51419770103157703, 9.386484678747171628 ) ) ;
#47681=DIRECTION ( 'NONE',  ( 0.000000000000000000, -2.173523156925980399E-06, 0.9999999999976378895 ) ) ;
#47682=CARTESIAN_POINT ( 'NONE',  ( -98.95846461277810135, -25.31200652517857819, 5.689168854314336166 ) ) ;
#47684=CARTESIAN_POINT ( 'NONE',  ( 18.16468007720714795, -9.286844270591712913, -1.500000000000002220 ) ) ;
#47685=ORIENTED_EDGE ( 'NONE', *, *, #90605, .F. ) ;
#47686=CARTESIAN_POINT ( 'NONE',  ( 14.37299948674089123, 17.95305339730678185, -1.500000000000002220 ) ) ;
#47687=CARTESIAN_POINT ( 'NONE',  ( -63.62287095715004881, -23.47593901973091235, -1.443836447539007972 ) ) ;
#47692=CARTESIAN_POINT ( 'NONE',  ( 17.95810460983813783, 11.44545274529666479, 11.49999999999999645 ) ) ;
#47695=CARTESIAN_POINT ( 'NONE',  ( 7.688942331755139747, 20.87172568467934752, -1.500000000000002220 ) ) ;
#47696=CARTESIAN_POINT ( 'NONE',  ( -12.00526669028610272, -16.82065764665920682, 11.49999999999998934 ) ) ;
#47697=VECTOR ( 'NONE', #56514, 1000.000000000000114 ) ;
#47699=ORIENTED_EDGE ( 'NONE', *, *, #47372, .T. ) ;
#47701=CARTESIAN_POINT ( 'NONE',  ( -95.58289840528635750, -25.00182538069147142, 7.747789668545044250 ) ) ;
#47703=LINE ( 'NONE', #64955, #99614 ) ;
#47704=ADVANCED_FACE ( 'NONE', ( #70791 ), #56580, .T. ) ;
#47705=ORIENTED_EDGE ( 'NONE', *, *, #38530, .F. ) ;
#47707=CARTESIAN_POINT ( 'NONE',  ( -70.56964911583740729, -25.12720894619000234, 7.077432069396976111 ) ) ;
#47708=CARTESIAN_POINT ( 'NONE',  ( 20.89859092893058801, 0.06103081833375877813, -1.500000000000002220 ) ) ;
#47709=CARTESIAN_POINT ( 'NONE',  ( 4.989390281198801347, -21.28523531580253803, 11.49999999999999645 ) ) ;
#47710=B_SPLINE_CURVE_WITH_KNOTS ( 'NONE', 3,
 ( #89312, #4078, #19781, #28904, #65502, #97418 ),
 .UNSPECIFIED., .F., .F.,
 ( 4, 2, 4 ),
 ( 0.000000000000000000, 0.001380901958385385509, 0.002761803916770771018 ),
 .UNSPECIFIED. ) ;
#47711=VECTOR ( 'NONE', #71529, 1000.000000000000114 ) ;
#47713=DIRECTION ( 'NONE',  ( -0.000000000000000000, 2.173523156925979552E-06, -0.9999999999976378895 ) ) ;
#47714=CARTESIAN_POINT ( 'NONE',  ( -11.50411854321151672, 19.32100693743031528, -1.500000000000002220 ) ) ;
#47717=CARTESIAN_POINT ( 'NONE',  ( -118.5578097239443025, -23.48786465467241769, 11.44779295918253581 ) ) ;
#47719=CARTESIAN_POINT ( 'NONE',  ( -31.52287095715006160, -24.64965694238574656, 8.947790433994207149 ) ) ;
#47720=ORIENTED_EDGE ( 'NONE', *, *, #37567, .T. ) ;
#47724=CARTESIAN_POINT ( 'NONE',  ( -18.57871158907727249, 10.67946855401146777, -1.500000000000002220 ) ) ;
#47725=CARTESIAN_POINT ( 'NONE',  ( -6.430504157862594994, -21.42354456762059201, 11.49999999999999645 ) ) ;
#47727=CARTESIAN_POINT ( 'NONE',  ( 18.99863377428308198, 9.053671573812124507, 11.49999999999998934 ) ) ;
#47728=CARTESIAN_POINT ( 'NONE',  ( -30.40154487420265994, -25.30206656716858404, 5.002391647799127483 ) ) ;
#47729=CARTESIAN_POINT ( 'NONE',  ( -19.80664267627650688, 2.137978742899185214, -1.500000000000002220 ) ) ;
#47730=CARTESIAN_POINT ( 'NONE',  ( -50.57411766822878718, -25.00182538069146432, 7.747789668545041586 ) ) ;
#47732=CARTESIAN_POINT ( 'NONE',  ( -7.037580251249667462, -20.86201633182841420, -1.500000000000002220 ) ) ;
#47733=FACE_OUTER_BOUND ( 'NONE', #41491, .T. ) ;
#47737=CARTESIAN_POINT ( 'NONE',  ( -54.52287095715006870, -23.47596703998600631, 11.44779298504229104 ) ) ;
#47738=CARTESIAN_POINT ( 'NONE',  ( -14.03827505669662479, 15.38897104800697591, 11.49999999999999645 ) ) ;
#47740=CARTESIAN_POINT ( 'NONE',  ( -111.5895376238167387, -23.48786465467241769, 11.44779295918254114 ) ) ;
#47743=CARTESIAN_POINT ( 'NONE',  ( -19.36244235409943926, 8.944087295975924334, 11.49999999999998934 ) ) ;
#47744=CARTESIAN_POINT ( 'NONE',  ( -53.62287095715005592, -29.50247984919015209, -1.443849546365058689 ) ) ;
#47745=CARTESIAN_POINT ( 'NONE',  ( -117.5228709571500048, -23.73934037231757443, 11.05740245334327732 ) ) ;
#47746=EDGE_CURVE ( 'NONE', #90318, #96355, #20595, .T. ) ;
#47747=CARTESIAN_POINT ( 'NONE',  ( -64.58349049003693665, -24.51419770103159124, 9.386484678747168076 ) ) ;
#47748=CARTESIAN_POINT ( 'NONE',  ( -71.31504266748430609, -25.30188801935125653, 5.302352381037461093 ) ) ;
#47749=CARTESIAN_POINT ( 'NONE',  ( 11.64696156460271581, 19.30390316350253244, -1.500000000000002220 ) ) ;
#47750=EDGE_CURVE ( 'NONE', #32461, #29559, #78815, .T. ) ;
#47753=B_SPLINE_CURVE_WITH_KNOTS ( 'NONE', 3,
 ( #49744, #26389, #57360, #88292 ),
 .UNSPECIFIED., .F., .F.,
 ( 4, 4 ),
 ( 0.1288497010136043508, 0.1298504480543696271 ),
 .UNSPECIFIED. ) ;
#47754=CARTESIAN_POINT ( 'NONE',  ( -79.00182917920848524, -25.29558293519123779, 5.503601469187146655 ) ) ;
#47755=CARTESIAN_POINT ( 'NONE',  ( -31.64312417419304424, -24.15620529776627379, 10.23563542870661536 ) ) ;
#47756=CARTESIAN_POINT ( 'NONE',  ( 0.7877182283408599162, 19.66719298131377514, 11.49999999999999645 ) ) ;
#47758=CARTESIAN_POINT ( 'NONE',  ( -77.52287095715006160, -29.50250243563736774, 8.947779886222141599 ) ) ;
#47759=VERTEX_POINT ( 'NONE', #94618 ) ;
#47761=CARTESIAN_POINT ( 'NONE',  ( -111.5228709571500332, -23.94994826722564696, -0.6494450866342719175 ) ) ;
#47762=CARTESIAN_POINT ( 'NONE',  ( -124.4728709571500360, -25.21147115331109489, 5.000950864497200499 ) ) ;
#47763=CARTESIAN_POINT ( 'NONE',  ( -48.52287095715006160, -29.50250786944525672, 11.44777988621624054 ) ) ;
#47766=CARTESIAN_POINT ( 'NONE',  ( 19.48663422773152121, -3.193742178437300794, -1.500000000000002220 ) ) ;
#47767=ADVANCED_FACE ( 'NONE', ( #3298 ), #12866, .F. ) ;
#47769=CARTESIAN_POINT ( 'NONE',  ( 19.91930514195032487, 3.327535025408205893, 11.49999999999999645 ) ) ;
#47771=VECTOR ( 'NONE', #68503, 1000.000000000000114 ) ;
#47774=CARTESIAN_POINT ( 'NONE',  ( -77.62287095715005592, -29.50250786944525672, 11.44777988621623521 ) ) ;
#47775=CARTESIAN_POINT ( 'NONE',  ( -81.42380231474228935, -25.30401792888237011, 5.197789011716578145 ) ) ;
#47777=FACE_OUTER_BOUND ( 'NONE', #74384, .T. ) ;
#47778=CARTESIAN_POINT ( 'NONE',  ( -59.22287095715007865, -23.47593901973090524, -1.443836447538997980 ) ) ;
#47779=DIRECTION ( 'NONE',  ( 1.000000000000000000, 3.773278334444167608E-23, 8.201307833595939069E-29 ) ) ;
#47780=CARTESIAN_POINT ( 'NONE',  ( 18.80801646011137507, -6.797914457553222434, 11.49999999999998934 ) ) ;
#47782=CARTESIAN_POINT ( 'NONE',  ( -34.55620429048339304, -24.64898659630528144, 1.056161002820817263 ) ) ;
#47783=CARTESIAN_POINT ( 'NONE',  ( -67.62287095715004170, -24.66019654487199020, 8.947790411086131712 ) ) ;
#47784=ORIENTED_EDGE ( 'NONE', *, *, #72627, .F. ) ;
#47785=EDGE_CURVE ( 'NONE', #61548, #93369, #87282, .T. ) ;
#47786=CARTESIAN_POINT ( 'NONE',  ( -79.55042822669543057, -24.15620529776628089, 10.23563542870660470 ) ) ;
#47787=CARTESIAN_POINT ( 'NONE',  ( -59.62287095715004881, -29.50250243563736774, 8.947779886222145151 ) ) ;
#47788=CARTESIAN_POINT ( 'NONE',  ( -125.6228709571500559, -24.99156045073393173, 7.747789690856161648 ) ) ;
#47789=CARTESIAN_POINT ( 'NONE',  ( -82.58953762381673869, -24.64965694238406968, 8.947790433994654791 ) ) ;
#47792=PLANE ( 'NONE',  #96544 ) ;
#47793=CARTESIAN_POINT ( 'NONE',  ( -73.62287095715005592, -24.65952944569304606, 1.056160979905698794 ) ) ;
#47794=VERTEX_POINT ( 'NONE', #27111 ) ;
#47795=CARTESIAN_POINT ( 'NONE',  ( 13.49383759531269433, -15.17088004136028090, 11.49999999999998934 ) ) ;
#47796=CARTESIAN_POINT ( 'NONE',  ( 5.514125806255895004E-17, -29.50248528299834305, 1.056150588822498460 ) ) ;
#47797=DIRECTION ( 'NONE',  ( 0.000000000000000000, 2.173523156925980399E-06, -0.9999999999976378895 ) ) ;
#47798=ORIENTED_EDGE ( 'NONE', *, *, #158, .F. ) ;
#47799=CARTESIAN_POINT ( 'NONE',  ( -50.40445135320379677, -25.26264178517331871, 7.101635255499235910 ) ) ;
#47800=CARTESIAN_POINT ( 'NONE',  ( -13.64458216870221818, 14.86554040878868044, -1.500000000000002220 ) ) ;
#47801=CARTESIAN_POINT ( 'NONE',  ( -11.89019930860364482, -17.45089671868802128, 11.49999999999999645 ) ) ;
#47803=CARTESIAN_POINT ( 'NONE',  ( 20.51613352552997327, 8.347415244503286758, 11.49999999999998934 ) ) ;
#47804=CARTESIAN_POINT ( 'NONE',  ( 11.93631617611541351, -16.73449621718459923, 11.49999999999998934 ) ) ;
#47808=CARTESIAN_POINT ( 'NONE',  ( -60.62287095715004881, -29.50249982740957577, 7.747779886224967605 ) ) ;
#47809=VERTEX_POINT ( 'NONE', #89014 ) ;
#47810=DIRECTION ( 'NONE',  ( -3.773278334453080206E-23, 0.9999999999976377785, 2.173523156925979975E-06 ) ) ;
#47813=ORIENTED_EDGE ( 'NONE', *, *, #70914, .F. ) ;
#47815=CARTESIAN_POINT ( 'NONE',  ( -112.6228709571501412, -23.96127896941632685, -0.6493128931037773777 ) ) ;
#47816=CARTESIAN_POINT ( 'NONE',  ( -127.6228709571500275, -24.66019654487199730, 8.947790411086121054 ) ) ;
#47818=CARTESIAN_POINT ( 'NONE',  ( 18.07348078632662691, -10.09602009226539288, -1.500000000000002220 ) ) ;
#47819=CARTESIAN_POINT ( 'NONE',  ( -12.04083774165243881, -18.01462592983040523, 11.49999999999999645 ) ) ;
#47820=ORIENTED_EDGE ( 'NONE', *, *, #42073, .T. ) ;
#47823=CARTESIAN_POINT ( 'NONE',  ( -111.6391784447225888, -25.23279326416602331, 3.670920698832722096 ) ) ;
#47824=CARTESIAN_POINT ( 'NONE',  ( -15.27869365379592281, -16.34152646814254339, 11.49999999999998934 ) ) ;
#47826=EDGE_CURVE ( 'NONE', #83609, #42451, #77562, .T. ) ;
#47827=CARTESIAN_POINT ( 'NONE',  ( -84.62287095715005592, -23.48783264082479150, -1.443836473390065489 ) ) ;
#47831=CARTESIAN_POINT ( 'NONE',  ( -35.48813154574202144, -24.40133493613049609, 9.663955038902800609 ) ) ;
#47833=ORIENTED_EDGE ( 'NONE', *, *, #45661, .T. ) ;
#47834=ORIENTED_EDGE ( 'NONE', *, *, #19135, .T. ) ;
#47836=CARTESIAN_POINT ( 'NONE',  ( -87.55620429048337883, -23.48786465467241058, 11.44779295918253936 ) ) ;
#47837=ORIENTED_EDGE ( 'NONE', *, *, #42705, .F. ) ;
#47838=DIRECTION ( 'NONE',  ( -1.000000000000000000, -3.773278334444167608E-23, -8.201307833595939069E-29 ) ) ;
#47839=CARTESIAN_POINT ( 'NONE',  ( -12.22836702412972087, 17.35733969022439993, -1.500000000000002220 ) ) ;
#47841=CARTESIAN_POINT ( 'NONE',  ( -50.52448634810669148, -25.00158670708910691, 2.256160236439223254 ) ) ;
#47842=CARTESIAN_POINT ( 'NONE',  ( -8.041798833237560729, -20.28069125152608976, -1.500000000000002220 ) ) ;
#47843=CARTESIAN_POINT ( 'NONE',  ( -88.88918693012689687, -25.22391110550272941, 6.409327647371936720 ) ) ;
#47846=CARTESIAN_POINT ( 'NONE',  ( 1.472770742059883897, 21.73951962378590963, -1.500000000000002220 ) ) ;
#47847=CARTESIAN_POINT ( 'NONE',  ( -30.57287095715007297, -24.38244319455381159, 0.3197473736007364065 ) ) ;
#47848=EDGE_LOOP ( 'NONE', ( #49470, #11625, #28788, #55856 ) ) ;
#47849=DIRECTION ( 'NONE',  ( -3.773278334444165844E-23, 1.000000000000000000, 0.000000000000000000 ) ) ;
#47850=CARTESIAN_POINT ( 'NONE',  ( -48.87675733776060838, -25.12782531155001919, 6.266175665688602514 ) ) ;
#47857=ORIENTED_EDGE ( 'NONE', *, *, #36961, .T. ) ;
#47858=EDGE_CURVE ( 'NONE', #39939, #72639, #19332, .T. ) ;
#47859=EDGE_LOOP ( 'NONE', ( #55312, #86653, #10778, #33319 ) ) ;
#47860=CARTESIAN_POINT ( 'NONE',  ( -27.97404546388469626, -24.80060134974466379, 2.305086465424985409 ) ) ;
#47861=CARTESIAN_POINT ( 'NONE',  ( -119.6228709571500559, -23.47593901973091235, -1.443836447538997536 ) ) ;
#47862=CARTESIAN_POINT ( 'NONE',  ( -21.08002519818654363, -2.465602145356518893, 11.49999999999998934 ) ) ;
#47864=CARTESIAN_POINT ( 'NONE',  ( -40.62287095715005592, -29.50248528299804818, 1.056150453629031594 ) ) ;
#47865=EDGE_CURVE ( 'NONE', #9142, #93778, #11383, .T. ) ;
#47868=CARTESIAN_POINT ( 'NONE',  ( -1.428710472040144452, 19.32843595812722626, 11.49999999999998934 ) ) ;
#47869=CARTESIAN_POINT ( 'NONE',  ( -117.5178510921751354, -24.35071581493544457, 9.817618358456019934 ) ) ;
#47870=VERTEX_POINT ( 'NONE', #34724 ) ;
#47871=CARTESIAN_POINT ( 'NONE',  ( -5.499840656826012975, 18.73951620154120334, 11.49999999999999645 ) ) ;
#47875=ADVANCED_FACE ( 'NONE', ( #38703 ), #15990, .T. ) ;
#47877=CARTESIAN_POINT ( 'NONE',  ( -89.64224457987518235, -23.48783264082478084, -1.443836473390068154 ) ) ;
#47878=CARTESIAN_POINT ( 'NONE',  ( -103.6228709571500559, -23.47593901973091235, -1.443836447539001089 ) ) ;
#47881=CARTESIAN_POINT ( 'NONE',  ( -18.74838588596843181, -5.942601993926947657, 11.49999999999998934 ) ) ;
#47882=VERTEX_POINT ( 'NONE', #69667 ) ;
#47883=AXIS2_PLACEMENT_3D ( 'NONE', #34188, #28072, #80350 ) ;
#47884=CARTESIAN_POINT ( 'NONE',  ( -11.65619939812097527, 18.16556634249905855, -1.500000000000002220 ) ) ;
#47886=CARTESIAN_POINT ( 'NONE',  ( -108.5228709571500616, -24.64898659630528854, 1.056161002820831474 ) ) ;
#47887=B_SPLINE_CURVE_WITH_KNOTS ( 'NONE', 3,
 ( #61622, #56891, #69721, #62114, #69212, #9693, #18801, #55887 ),
 .UNSPECIFIED., .F., .F.,
 ( 4, 2, 2, 4 ),
 ( 6.391158118969102054E-06, 0.002007136338672930488, 0.003007508928949909066, 0.004007881519226887644 ),
 .UNSPECIFIED. ) ;
#47889=CARTESIAN_POINT ( 'NONE',  ( -125.5228709571501469, -24.92604778743018912, 8.074972756849362554 ) ) ;
#47891=CARTESIAN_POINT ( 'NONE',  ( -97.58660980088102121, -24.51419770103157703, 9.386484678747176957 ) ) ;
#47895=FACE_OUTER_BOUND ( 'NONE', #48880, .T. ) ;
#47896=CARTESIAN_POINT ( 'NONE',  ( -73.52287095715007581, -23.48786465467241058, 11.44779295918254647 ) ) ;
#47897=CARTESIAN_POINT ( 'NONE',  ( -114.5916529831659858, -23.96169478059714208, 10.65365249895717170 ) ) ;
#47898=CARTESIAN_POINT ( 'NONE',  ( 10.08953278062578462, 17.19620541797624824, -1.500000000000002220 ) ) ;
#47899=DIRECTION ( 'NONE',  ( -3.773278334444167608E-23, 1.000000000000000000, 0.000000000000000000 ) ) ;
#47900=CARTESIAN_POINT ( 'NONE',  ( -3.387584560642538101, 19.54024307811383210, -1.500000000000002220 ) ) ;
#47901=ORIENTED_EDGE ( 'NONE', *, *, #89661, .F. ) ;
#47905=CARTESIAN_POINT ( 'NONE',  ( 20.56943099487245519, -2.726235779781958968, 11.49999999999999645 ) ) ;
#47906=CARTESIAN_POINT ( 'NONE',  ( -127.4728709571500360, -29.48149383318413541, 5.000941581248043555 ) ) ;
#47907=DIRECTION ( 'NONE',  ( -3.773278334444167608E-23, 1.000000000000000000, 0.000000000000000000 ) ) ;
#47908=CARTESIAN_POINT ( 'NONE',  ( -20.44213351528904354, 10.05872170072450977, 11.49999999999999645 ) ) ;
#47911=CARTESIAN_POINT ( 'NONE',  ( -57.62287095715004881, -23.73907113216990794, -1.053371485793229922 ) ) ;
#47912=CARTESIAN_POINT ( 'NONE',  ( -100.5895376238167245, -25.00158670708909270, 2.256160236439166411 ) ) ;
#47913=EDGE_LOOP ( 'NONE', ( #96860, #94582, #21206, #3175 ) ) ;
#47915=CARTESIAN_POINT ( 'NONE',  ( -2.107266074560359748, -20.09985696230311447, -1.500000000000002220 ) ) ;
#47920=ORIENTED_EDGE ( 'NONE', *, *, #91901, .T. ) ;
#47922=CARTESIAN_POINT ( 'NONE',  ( -13.60431050971674694, 18.46711184989817411, -1.500000000000002220 ) ) ;
#47923=CARTESIAN_POINT ( 'NONE',  ( -84.52287095715001897, -23.95044443724990657, 10.65354141964648704 ) ) ;
#47924=CARTESIAN_POINT ( 'NONE',  ( 10.22567584263966722, 17.17405255344276682, -1.500000000000002220 ) ) ;
#47926=CARTESIAN_POINT ( 'NONE',  ( 4.154569570224219355, 20.57273982587956240, 11.49999999999999645 ) ) ;
#47927=DIRECTION ( 'NONE',  ( 0.000000000000000000, 0.9999999999976377785, 2.173523156925979128E-06 ) ) ;
#47928=CARTESIAN_POINT ( 'NONE',  ( -114.6228709571500701, -23.47596703998600631, 11.44779298504227860 ) ) ;
#47929=CARTESIAN_POINT ( 'NONE',  ( 13.62230711432095553, -17.35066874027886286, -1.500000000000002220 ) ) ;
#47931=ORIENTED_EDGE ( 'NONE', *, *, #46246, .T. ) ;
#47933=CARTESIAN_POINT ( 'NONE',  ( -49.50910156767503878, -25.18440247356948447, 3.963069022222974969 ) ) ;
#47934=DIRECTION ( 'NONE',  ( -0.000000000000000000, 2.173523156925979552E-06, -0.9999999999976378895 ) ) ;
#47944=CARTESIAN_POINT ( 'NONE',  ( 14.40702264168333890, -14.58922348230443689, -1.500000000000002220 ) ) ;
#47945=EDGE_CURVE ( 'NONE', #15171, #95755, #85375, .T. ) ;
#47946=ORIENTED_EDGE ( 'NONE', *, *, #76788, .T. ) ;
#47947=CARTESIAN_POINT ( 'NONE',  ( -60.52287095715006160, -29.50250786944525672, 11.44777988621623876 ) ) ;
#47950=CARTESIAN_POINT ( 'NONE',  ( -20.55991158545366204, 8.586518200734140294, -1.500000000000002220 ) ) ;
#47951=ADVANCED_FACE ( 'NONE', ( #36719 ), #68621, .T. ) ;
#47952=B_SPLINE_CURVE_WITH_KNOTS ( 'NONE', 3,
 ( #80395, #10885, #99092, #7245 ),
 .UNSPECIFIED., .F., .F.,
 ( 4, 4 ),
 ( 0.000000000000000000, 0.0001000000000000028644 ),
 .UNSPECIFIED. ) ;
#47955=ORIENTED_EDGE ( 'NONE', *, *, #44736, .F. ) ;
#47956=CARTESIAN_POINT ( 'NONE',  ( -96.62287095715009855, -24.34917612406837861, 0.1852690917426671191 ) ) ;
#47957=CARTESIAN_POINT ( 'NONE',  ( -124.6228709571499991, -23.94994826722566117, -0.6494450866342683648 ) ) ;
#47958=CARTESIAN_POINT ( 'NONE',  ( 16.93201058511109380, 12.15574511561022852, -1.500000000000002220 ) ) ;
#47959=VERTEX_POINT ( 'NONE', #16869 ) ;
#47961=ORIENTED_EDGE ( 'NONE', *, *, #78741, .F. ) ;
#47963=CARTESIAN_POINT ( 'NONE',  ( -104.2228709571500787, -23.47593901973090524, -1.443836447538996648 ) ) ;
#47964=CARTESIAN_POINT ( 'NONE',  ( 17.27681320446407298, 11.92757687370068886, -1.500000000000002220 ) ) ;
#47965=VERTEX_POINT ( 'NONE', #46832 ) ;
#47966=CARTESIAN_POINT ( 'NONE',  ( -118.5228709571500758, -24.64965694238408034, 8.947790433994191162 ) ) ;
#47967=CARTESIAN_POINT ( 'NONE',  ( -37.52287095715008292, -23.72773821059537269, 11.05748984161097326 ) ) ;
#47969=CARTESIAN_POINT ( 'NONE',  ( -86.62887336595798615, -24.35071581493543391, 9.817618358456027039 ) ) ;
#47970=CARTESIAN_POINT ( 'NONE',  ( -59.55363052684328551, -23.96119346886879597, -0.6495511937832131322 ) ) ;
#47971=DIRECTION ( 'NONE',  ( -3.773278334444166432E-23, 1.000000000000000000, 0.000000000000000000 ) ) ;
#47973=CARTESIAN_POINT ( 'NONE',  ( -21.66996937300057269, -4.939502015459471096, 11.49999999999999645 ) ) ;
#47974=ORIENTED_EDGE ( 'NONE', *, *, #38773, .T. ) ;
#47976=CARTESIAN_POINT ( 'NONE',  ( -87.52287095715006160, -23.73907113217651599, -1.053371485781588124 ) ) ;
#47978=CARTESIAN_POINT ( 'NONE',  ( -15.33504971967173702, 16.71734053393862496, 11.49999999999998934 ) ) ;
#47980=CARTESIAN_POINT ( 'NONE',  ( -87.62287095715004170, -24.66019654487199020, 8.947790411086129936 ) ) ;
#47981=ORIENTED_EDGE ( 'NONE', *, *, #50040, .F. ) ;
#47982=EDGE_CURVE ( 'NONE', #30802, #20834, #36240, .T. ) ;
#47983=ORIENTED_EDGE ( 'NONE', *, *, #47496, .F. ) ;
#47986=CARTESIAN_POINT ( 'NONE',  ( 19.08902475966321788, 6.433202353099247262, 11.49999999999998934 ) ) ;
#47991=CARTESIAN_POINT ( 'NONE',  ( 11.21425909587273928, 19.38466839394011387, -1.500000000000002220 ) ) ;
#47994=VERTEX_POINT ( 'NONE', #94495 ) ;
#47995=ORIENTED_EDGE ( 'NONE', *, *, #37292, .T. ) ;
#47997=CARTESIAN_POINT ( 'NONE',  ( -94.63646352547178253, -23.73791477778912196, 11.05961554403170588 ) ) ;
#47998=CARTESIAN_POINT ( 'NONE',  ( -110.6228709571500701, -25.00182538069145011, 7.747789668545099317 ) ) ;
#48000=VECTOR ( 'NONE', #8342, 1000.000000000000114 ) ;
#48001=FACE_BOUND ( 'NONE', #46951, .T. ) ;
#48002=EDGE_CURVE ( 'NONE', #37139, #59253, #71671, .T. ) ;
#48003=CARTESIAN_POINT ( 'NONE',  ( -13.92019785312828972, -13.74635529968554515, -1.500000000000002220 ) ) ;
#48006=CARTESIAN_POINT ( 'NONE',  ( -0.9917595143200197416, 21.46465604038169772, 11.49999999999998934 ) ) ;
#48007=CARTESIAN_POINT ( 'NONE',  ( -42.52287095715005449, -23.48786465467240347, 11.44779295918255180 ) ) ;
#48008=CARTESIAN_POINT ( 'NONE',  ( -54.62287095715006302, -23.95044443724992078, 10.65354141964649592 ) ) ;
#48009=CARTESIAN_POINT ( 'NONE',  ( -123.5228709571500758, -23.96177878511309345, 10.65340807706328441 ) ) ;
#48010=EDGE_CURVE ( 'NONE', #39962, #20337, #67700, .T. ) ;
#48012=CARTESIAN_POINT ( 'NONE',  ( -20.38739128398232836, 10.50225141308550292, -1.500000000000002220 ) ) ;
#48014=CARTESIAN_POINT ( 'NONE',  ( -93.62287095715004170, -23.48783264082478794, -1.443836473390063713 ) ) ;
#48015=CARTESIAN_POINT ( 'NONE',  ( -53.59900199587650604, -23.96119346886879953, -0.6495511937832126881 ) ) ;
#48016=CARTESIAN_POINT ( 'NONE',  ( 12.85705330080557829, 15.37097598829428513, 11.49999999999999645 ) ) ;
#48017=CARTESIAN_POINT ( 'NONE',  ( -79.55512035851637620, -25.31594366164218712, 4.736589999760145275 ) ) ;
#48021=B_SPLINE_CURVE_WITH_KNOTS ( 'NONE', 3,
 ( #48276, #94940, #56403, #95441 ),
 .UNSPECIFIED., .F., .F.,
 ( 4, 4 ),
 ( 0.4190663428356088405, 0.4200670898763741445 ),
 .UNSPECIFIED. ) ;
#48023=CARTESIAN_POINT ( 'NONE',  ( -7.892909027492730267, -20.28523913882780505, -1.500000000000002220 ) ) ;
#48024=FACE_OUTER_BOUND ( 'NONE', #52345, .T. ) ;
#48025=CARTESIAN_POINT ( 'NONE',  ( 2.166912399371504705, 19.51343182558466793, -1.500000000000002220 ) ) ;
#48027=CARTESIAN_POINT ( 'NONE',  ( -100.6228709571500559, -24.99132157543167310, 2.256160258750667502 ) ) ;
#48028=CARTESIAN_POINT ( 'NONE',  ( -109.5669895805274336, -25.27925804186644498, 4.843009203900840554 ) ) ;
#48030=DIRECTION ( 'NONE',  ( 1.000000000000000000, 3.773278334444166432E-23, 8.201307841325785021E-29 ) ) ;
#48032=CARTESIAN_POINT ( 'NONE',  ( 0.1292827521129817636, -20.55975067039486603, 11.49999999999999645 ) ) ;
#48034=CARTESIAN_POINT ( 'NONE',  ( -120.6241461665311192, -24.83618233451451118, 1.606449574219542598 ) ) ;
#48035=CARTESIAN_POINT ( 'NONE',  ( -3.801653518169780366, -22.29579330195574016, 11.49999999999999645 ) ) ;
#48036=ORIENTED_EDGE ( 'NONE', *, *, #55296, .F. ) ;
#48037=CARTESIAN_POINT ( 'NONE',  ( -70.03562343076868046, -25.12219137083621590, 7.066379050738610168 ) ) ;
#48039=CARTESIAN_POINT ( 'NONE',  ( -125.5888992149329653, -24.92592662359561828, 8.075495903018000021 ) ) ;
#48041=CARTESIAN_POINT ( 'NONE',  ( -33.62287095715005592, -23.47593901973091235, -1.443836447539013301 ) ) ;
#48044=VERTEX_POINT ( 'NONE', #33102 ) ;
#48045=CARTESIAN_POINT ( 'NONE',  ( -79.34938298551102775, -25.26750068962975604, 5.853656373955819170 ) ) ;
#48046=CARTESIAN_POINT ( 'NONE',  ( 22.79674358141071977, 1.614764915196592598, -1.500000000000002220 ) ) ;
#48048=CARTESIAN_POINT ( 'NONE',  ( -96.62549120092178612, -24.51314013834316086, 0.6176544820404182845 ) ) ;
#48049=CARTESIAN_POINT ( 'NONE',  ( -63.54868262085074093, -24.15620529776628089, 10.23563542870660470 ) ) ;
#48050=CARTESIAN_POINT ( 'NONE',  ( 5.133194422563156500, 21.89913303424002677, 11.49999999999999645 ) ) ;
#48051=ORIENTED_EDGE ( 'NONE', *, *, #57111, .F. ) ;
#48053=CARTESIAN_POINT ( 'NONE',  ( -13.81295463269534096, 17.03802364079049525, 11.49999999999998934 ) ) ;
#48054=CARTESIAN_POINT ( 'NONE',  ( -127.4728709571500360, -25.40558663563398767, 5.000950440326727531 ) ) ;
#48056=CARTESIAN_POINT ( 'NONE',  ( -34.55278932522879387, -23.96169478059712077, 10.65365249895718769 ) ) ;
#48057=CARTESIAN_POINT ( 'NONE',  ( -121.5228709571500474, -23.95044443724993144, 10.65354141964648704 ) ) ;
#48058=ORIENTED_EDGE ( 'NONE', *, *, #76677, .F. ) ;
#48059=CARTESIAN_POINT ( 'NONE',  ( -116.6228709571500417, -24.66019654487199730, 8.947790411086121054 ) ) ;
#48063=EDGE_CURVE ( 'NONE', #623, #39855, #91936, .T. ) ;
#48064=CARTESIAN_POINT ( 'NONE',  ( -9.379331868514380943, 18.20734191464070406, -1.500000000000002220 ) ) ;
#48067=VERTEX_POINT ( 'NONE', #23975 ) ;
#48068=VERTEX_POINT ( 'NONE', #64080 ) ;
#48070=CARTESIAN_POINT ( 'NONE',  ( 19.40787663092975279, -12.54570180764831377, 11.49999999999998934 ) ) ;
#48071=FACE_OUTER_BOUND ( 'NONE', #87493, .T. ) ;
#48072=CARTESIAN_POINT ( 'NONE',  ( 6.844040470191356640, -19.11863935190610064, -1.500000000000002220 ) ) ;
#48075=PLANE ( 'NONE',  #73634 ) ;
#48076=CARTESIAN_POINT ( 'NONE',  ( -92.51846584691269015, -23.73766607897670866, -1.055555164236430032 ) ) ;
#48078=ADVANCED_FACE ( 'NONE', ( #96002 ), #88392, .F. ) ;
#48079=CARTESIAN_POINT ( 'NONE',  ( -93.62287095715007013, -24.33927499327855415, 9.819080762295811837 ) ) ;
#48081=CARTESIAN_POINT ( 'NONE',  ( 5.543860000110784725, 20.76261553274053284, 11.49999999999999645 ) ) ;
#48083=CARTESIAN_POINT ( 'NONE',  ( -75.63649189368283032, -24.40034930558991633, 0.3402023900116103450 ) ) ;
#48084=CARTESIAN_POINT ( 'NONE',  ( -112.6228709571500559, -24.64898659630368272, 1.056161002820831474 ) ) ;
#48085=EDGE_CURVE ( 'NONE', #14129, #82898, #44683, .T. ) ;
#48086=VERTEX_POINT ( 'NONE', #89886 ) ;
#48087=EDGE_CURVE ( 'NONE', #65800, #41620, #96803, .T. ) ;
#48088=CARTESIAN_POINT ( 'NONE',  ( 10.28901978357889035, -18.02705789925236957, -1.500000000000002220 ) ) ;
#48089=ORIENTED_EDGE ( 'NONE', *, *, #86604, .T. ) ;
#48090=CARTESIAN_POINT ( 'NONE',  ( -125.5200017711960783, -24.63355581998386512, 0.9682620441944075340 ) ) ;
#48091=ORIENTED_EDGE ( 'NONE', *, *, #29190, .T. ) ;
#48093=CARTESIAN_POINT ( 'NONE',  ( -53.52287095715004739, -23.73907113216989373, -1.053371485793253237 ) ) ;
#48094=EDGE_LOOP ( 'NONE', ( #87316, #34613, #35755, #35185 ) ) ;
#48096=CARTESIAN_POINT ( 'NONE',  ( -48.52287095715007581, -23.47593901973090524, -1.443836447538997314 ) ) ;
#48097=CARTESIAN_POINT ( 'NONE',  ( -42.49911757110140798, -24.15620529776627734, 10.23563542870661358 ) ) ;
#48098=EDGE_CURVE ( 'NONE', #35626, #17176, #95539, .T. ) ;
#48099=DIRECTION ( 'NONE',  ( -1.000000000000000000, -3.773278334444166432E-23, -8.201307841325785021E-29 ) ) ;
#48100=CARTESIAN_POINT ( 'NONE',  ( 7.103389721457689099, 20.86620700561973862, 11.49999999999999645 ) ) ;
#48103=CARTESIAN_POINT ( 'NONE',  ( -9.785633969878258398, 20.35780147342342516, 11.49999999999998934 ) ) ;
#48104=VECTOR ( 'NONE', #47580, 1000.000000000000114 ) ;
#48105=CARTESIAN_POINT ( 'NONE',  ( -7.324709186033012465, -19.69651249574825513, -1.500000000000002220 ) ) ;
#48113=CARTESIAN_POINT ( 'NONE',  ( 14.81885032312887240, -15.09863332352077592, 11.49999999999998934 ) ) ;
#48114=CARTESIAN_POINT ( 'NONE',  ( -66.62287095715002749, -24.33927499327853639, 9.819080762295815390 ) ) ;
#48115=CARTESIAN_POINT ( 'NONE',  ( -58.85574863676698953, -25.33009847151394922, 4.495758292450050320 ) ) ;
#48118=LINE ( 'NONE', #39497, #16226 ) ;
#48119=CARTESIAN_POINT ( 'NONE',  ( -13.56020932195406203, -17.60290058955388659, -1.500000000000002220 ) ) ;
#48120=CARTESIAN_POINT ( 'NONE',  ( -114.6292325214853491, -23.73766607897672287, -1.055555164236428700 ) ) ;
#48121=ADVANCED_FACE ( 'NONE', ( #19860 ), #49345, .F. ) ;
#48124=CARTESIAN_POINT ( 'NONE',  ( -37.58686907815667411, -24.34968618360933590, 0.1864209137778856384 ) ) ;
#48126=VECTOR ( 'NONE', #39383, 1000.000000000000114 ) ;
#48127=CARTESIAN_POINT ( 'NONE',  ( -41.80098236575750548, -25.24187400068776554, 3.756537540763403182 ) ) ;
#48129=CARTESIAN_POINT ( 'NONE',  ( -12.17249226084429203, 15.20430173202493940, -1.500000000000002220 ) ) ;
#48130=CARTESIAN_POINT ( 'NONE',  ( -20.78045986758521835, -5.208592277829342088, -1.500000000000002220 ) ) ;
#48133=CARTESIAN_POINT ( 'NONE',  ( -51.62368720275268430, -24.65952944569304250, 1.056160979905695463 ) ) ;
#48134=CARTESIAN_POINT ( 'NONE',  ( -100.5840138597264826, -25.27359975741654807, 3.299225944038700398 ) ) ;
#48135=CARTESIAN_POINT ( 'NONE',  ( -21.69093436787670726, -6.948586514802197023, -1.500000000000002220 ) ) ;
#48138=AXIS2_PLACEMENT_3D ( 'NONE', #8525, #48099, #40480 ) ;
#48139=CARTESIAN_POINT ( 'NONE',  ( -99.52287095715006160, -23.47596703998600631, 11.44779298504228215 ) ) ;
#48140=CARTESIAN_POINT ( 'NONE',  ( -106.5228709571500758, -24.64965694238408034, 8.947790433994192938 ) ) ;
#48141=CARTESIAN_POINT ( 'NONE',  ( -15.96263503330635380, 11.84234753045382682, 11.49999999999999645 ) ) ;
#48142=CARTESIAN_POINT ( 'NONE',  ( -84.52287095715006160, -23.96127896941631974, -0.6493128931038028018 ) ) ;
#48144=CARTESIAN_POINT ( 'NONE',  ( -112.6228709571500559, -23.47596703998600631, 11.44779298504227860 ) ) ;
#48145=CARTESIAN_POINT ( 'NONE',  ( -65.22287095715006444, -23.47593901973090169, -1.443836447538997536 ) ) ;
#48148=EDGE_CURVE ( 'NONE', #13213, #3403, #14475, .T. ) ;
#48151=CARTESIAN_POINT ( 'NONE',  ( -21.58526226860004371, 1.989002153404973328, -1.500000000000002220 ) ) ;
#48152=CARTESIAN_POINT ( 'NONE',  ( -84.52287095715007581, -24.66019654487199730, 8.947790411086122830 ) ) ;
#48153=CARTESIAN_POINT ( 'NONE',  ( 13.27039818535887505, -14.28956163997708906, -1.500000000000002220 ) ) ;
#48154=DIRECTION ( 'NONE',  ( 0.000000000000000000, 0.9999999999976377785, 2.173523156925979975E-06 ) ) ;
#48156=CARTESIAN_POINT ( 'NONE',  ( -5.548086588741434788, -19.59138962566686004, 11.49999999999999645 ) ) ;
#48162=CARTESIAN_POINT ( 'NONE',  ( -39.36780865613509661, -25.31628669946116617, 5.233841552006910369 ) ) ;
#48163=FACE_OUTER_BOUND ( 'NONE', #96322, .T. ) ;
#48164=DIRECTION ( 'NONE',  ( -3.773278334453079030E-23, 0.9999999999976377785, 2.173523156925979128E-06 ) ) ;
#48165=CARTESIAN_POINT ( 'NONE',  ( 19.99232773509726258, 2.034096180923423702, 11.49999999999998934 ) ) ;
#48167=EDGE_LOOP ( 'NONE', ( #95719, #68371, #12476, #87663 ) ) ;
#48168=PLANE ( 'NONE',  #85281 ) ;
#48170=CARTESIAN_POINT ( 'NONE',  ( 19.00551534866085746, 12.86435971046890359, 11.49999999999999645 ) ) ;
#48171=CARTESIAN_POINT ( 'NONE',  ( -2.780358639097238349, 22.57001311929844434, 11.49999999999998934 ) ) ;
#48172=ORIENTED_EDGE ( 'NONE', *, *, #95, .F. ) ;
#48173=CARTESIAN_POINT ( 'NONE',  ( -30.47287095715007510, -23.47596699454220470, 11.42688508591989560 ) ) ;
#48174=B_SPLINE_CURVE_WITH_KNOTS ( 'NONE', 3,
 ( #38563, #23828, #10993, #26719, #69518, #100420, #46686, #58668 ),
 .UNSPECIFIED., .F., .F.,
 ( 4, 2, 2, 4 ),
 ( -0.001240666984355842791, -0.0002401179793395018334, 0.0007604310256768391247, 0.002761529035709520824 ),
 .UNSPECIFIED. ) ;
#48175=CARTESIAN_POINT ( 'NONE',  ( -98.52287095715000476, -23.73907113216990084, -1.053371485793250351 ) ) ;
#48176=CARTESIAN_POINT ( 'NONE',  ( -90.54958004235005831, -24.40034930558990922, 0.3402023900116079580 ) ) ;
#48178=CARTESIAN_POINT ( 'NONE',  ( -61.24303164512834030, -25.04307381209219230, 7.563174986197129357 ) ) ;
#48179=CARTESIAN_POINT ( 'NONE',  ( -69.54471688719442568, -24.35071581493542681, 9.817618358456032368 ) ) ;
#48181=CARTESIAN_POINT ( 'NONE',  ( -122.5185787333176108, -24.65952944569305316, 1.056160979905708786 ) ) ;
#48182=CARTESIAN_POINT ( 'NONE',  ( -58.55986403960651643, -23.73766607897670156, -1.055555164236457344 ) ) ;
#48183=VERTEX_POINT ( 'NONE', #51329 ) ;
#48184=CARTESIAN_POINT ( 'NONE',  ( -6.692510123977180925, 19.25193956699996178, -1.500000000000002220 ) ) ;
#48185=ORIENTED_EDGE ( 'NONE', *, *, #79345, .T. ) ;
#48187=CARTESIAN_POINT ( 'NONE',  ( -19.49525799874905729, 12.17417675796824561, -1.500000000000002220 ) ) ;
#48188=CARTESIAN_POINT ( 'NONE',  ( -39.52287095715008292, -23.48783264082476308, -1.443836473390098574 ) ) ;
#48192=CARTESIAN_POINT ( 'NONE',  ( -86.62287095715004170, -29.50248528299804818, 1.056150453629040253 ) ) ;
#48194=CARTESIAN_POINT ( 'NONE',  ( -119.4337121810133198, -25.30063765797860498, 5.393961676144591877 ) ) ;
#48195=CARTESIAN_POINT ( 'NONE',  ( -14.61619677566029729, 15.53698580111986693, 11.49999999999999645 ) ) ;
#48196=ORIENTED_EDGE ( 'NONE', *, *, #32145, .T. ) ;
#48199=CARTESIAN_POINT ( 'NONE',  ( -13.56020932195406203, -17.60290058955388659, 11.49999999999998934 ) ) ;
#48200=EDGE_CURVE ( 'NONE', #26747, #39067, #73665, .T. ) ;
#48201=CARTESIAN_POINT ( 'NONE',  ( -10.67548511050313209, -17.69376651829569269, 11.49999999999998934 ) ) ;
#48203=VERTEX_POINT ( 'NONE', #5149 ) ;
#48205=CARTESIAN_POINT ( 'NONE',  ( -95.63507531277841167, -24.15602025860896163, 10.28564288303536856 ) ) ;
#48206=ORIENTED_EDGE ( 'NONE', *, *, #11963, .T. ) ;
#48207=CARTESIAN_POINT ( 'NONE',  ( -95.52287095715006160, -24.99132157543166954, 2.256160258750667502 ) ) ;
#48211=CARTESIAN_POINT ( 'NONE',  ( -70.38569055212785486, -25.12330845317594807, 7.099802567542052856 ) ) ;
#48212=CARTESIAN_POINT ( 'NONE',  ( -19.85847575633505713, -6.422239212204448044, -1.500000000000002220 ) ) ;
#48213=ADVANCED_FACE ( 'NONE', ( #42243 ), #65409, .T. ) ;
#48214=CARTESIAN_POINT ( 'NONE',  ( -20.57666286913221754, 7.287794730890116313, 11.49999999999999645 ) ) ;
#48215=CARTESIAN_POINT ( 'NONE',  ( -102.6228709571500701, -24.66019654487199730, 8.947790411086121054 ) ) ;
#48217=CARTESIAN_POINT ( 'NONE',  ( 8.413247042826936806, 20.86129769029627923, -1.500000000000002220 ) ) ;
#48218=CARTESIAN_POINT ( 'NONE',  ( -118.5566399574894945, -23.73791477778912551, 11.05961554403169878 ) ) ;
#48222=ORIENTED_EDGE ( 'NONE', *, *, #15520, .T. ) ;
#48223=VERTEX_POINT ( 'NONE', #4659 ) ;
#48224=CARTESIAN_POINT ( 'NONE',  ( -35.62287095715005592, -25.00182538069145011, 7.747789668545097541 ) ) ;
#48226=CARTESIAN_POINT ( 'NONE',  ( -13.99230614532761052, -16.21612836239924960, -1.500000000000002220 ) ) ;
#48227=CARTESIAN_POINT ( 'NONE',  ( -11.14805103425725719, -19.39388463112642214, 11.49999999999999645 ) ) ;
#48230=CARTESIAN_POINT ( 'NONE',  ( 20.15827220212406701, 6.050813824765241655, -1.500000000000002220 ) ) ;
#48231=CARTESIAN_POINT ( 'NONE',  ( -30.42284766947733488, -24.74885280525437992, 8.640462295247351321 ) ) ;
#48232=CARTESIAN_POINT ( 'NONE',  ( -3.169371320753151977, 19.67850563098683736, -1.500000000000002220 ) ) ;
#48233=CARTESIAN_POINT ( 'NONE',  ( -117.6228709571500559, -23.96127896941633750, -0.6493128931037767115 ) ) ;
#48235=CARTESIAN_POINT ( 'NONE',  ( -21.77411086464670831, -3.637377321037103872, -1.500000000000002220 ) ) ;
#48236=EDGE_LOOP ( 'NONE', ( #84612, #44254, #44770, #74139 ) ) ;
#48237=CARTESIAN_POINT ( 'NONE',  ( -116.5567473932748044, -23.73766607897671577, -1.055555164236427812 ) ) ;
#48239=CARTESIAN_POINT ( 'NONE',  ( -18.77111393065419875, 9.022841878967760465, 11.49999999999999645 ) ) ;
#48241=EDGE_CURVE ( 'NONE', #93369, #10565, #58000, .T. ) ;
#48243=DIRECTION ( 'NONE',  ( 0.000000000000000000, 0.9999999999976377785, 2.173523156925979128E-06 ) ) ;
#48245=CARTESIAN_POINT ( 'NONE',  ( -48.52287095715007581, -23.47593901973090524, -1.443836447538997314 ) ) ;
#48246=CARTESIAN_POINT ( 'NONE',  ( -20.14006130340733236, -7.001243683211865410, 11.49999999999998934 ) ) ;
#48247=CARTESIAN_POINT ( 'NONE',  ( -40.52287095715005449, -29.50248789122583659, 2.256150453626215580 ) ) ;
#48248=CARTESIAN_POINT ( 'NONE',  ( -50.45707490627877689, -25.19522716123442407, 3.295339427985402025 ) ) ;
#48249=EDGE_CURVE ( 'NONE', #80353, #40608, #73795, .T. ) ;
#48250=CARTESIAN_POINT ( 'NONE',  ( -128.5228709571500758, -23.47593901973090524, -1.443836447538996204 ) ) ;
#48251=CARTESIAN_POINT ( 'NONE',  ( -69.99341794969650721, -25.22594453560301631, 6.517383687127669134 ) ) ;
#48252=CARTESIAN_POINT ( 'NONE',  ( -22.55165446212525993, 1.111233042438415808, -1.500000000000002220 ) ) ;
#48253=B_SPLINE_SURFACE_WITH_KNOTS ( 'NONE', 3, 3, ( 
 ( #77869, #94104, #31715, #69784 ),
 ( #47445, #7368, #84995, #84500 ),
 ( #78869, #39320, #71283, #93103 ),
 ( #38821, #32709, #63180, #93598 ),
 ( #23584, #16982, #261, #9370 ),
 ( #54554, #78373, #24591, #69280 ),
 ( #16474, #1277, #8878, #63691 ) ),
 .UNSPECIFIED., .F., .F., .F.,
 ( 4, 3, 4 ),
 ( 4, 4 ),
 ( 0.0004766839783817236630, 0.1029713700210892063, 0.2054660560637966982 ),
 ( 0.8597126934696902589, 0.8611220878828262926 ),
 .UNSPECIFIED. ) ;
#48255=ORIENTED_EDGE ( 'NONE', *, *, #66085, .T. ) ;
#48256=CARTESIAN_POINT ( 'NONE',  ( -51.48758594601332561, -25.28167085146487381, 5.912859751850549905 ) ) ;
#48257=CARTESIAN_POINT ( 'NONE',  ( -31.63563380732087893, -24.35071581493542325, 9.817618358456039473 ) ) ;
#48258=CARTESIAN_POINT ( 'NONE',  ( 14.14096853472169535, -13.71769858867784464, 11.49999999999999645 ) ) ;
#48259=CARTESIAN_POINT ( 'NONE',  ( -49.52287095715004739, -24.33832256527048798, 0.1851278514138550435 ) ) ;
#48261=ORIENTED_EDGE ( 'NONE', *, *, #95135, .F. ) ;
#48262=CARTESIAN_POINT ( 'NONE',  ( -111.5228709571501042, -23.72747288104470087, -1.053458166803224794 ) ) ;
#48263=CARTESIAN_POINT ( 'NONE',  ( -99.52764846858842418, -29.50249168100820896, 3.999763059310747160 ) ) ;
#48264=CARTESIAN_POINT ( 'NONE',  ( -124.5206801752270422, -24.15620529776629510, 10.23563542870659404 ) ) ;
#48267=CARTESIAN_POINT ( 'NONE',  ( -57.62287095715004881, -23.47593901973091235, -1.443836447539007972 ) ) ;
#48268=CARTESIAN_POINT ( 'NONE',  ( 18.87426695099163254, 5.791883100666666451, 11.49999999999998934 ) ) ;
#48270=CARTESIAN_POINT ( 'NONE',  ( 18.20877288740043198, -8.745817889818592761, 11.49999999999999645 ) ) ;
#48272=EDGE_CURVE ( 'NONE', #53585, #85354, #14242, .T. ) ;
#48274=ORIENTED_EDGE ( 'NONE', *, *, #35696, .T. ) ;
#48275=PLANE ( 'NONE',  #41056 ) ;
#48276=CARTESIAN_POINT ( 'NONE',  ( -72.52287095715007581, -23.47596703998600631, 11.44779298504228748 ) ) ;
#48277=DIRECTION ( 'NONE',  ( -3.773278334453079030E-23, 0.9999999999976377785, 2.173523156925979128E-06 ) ) ;
#48278=PLANE ( 'NONE',  #25677 ) ;
#48280=CARTESIAN_POINT ( 'NONE',  ( -103.6228709571500559, -24.64965695001469115, 8.947790433994178727 ) ) ;
#48281=B_SPLINE_CURVE_WITH_KNOTS ( 'NONE', 3,
 ( #74788, #11408, #36739, #20012 ),
 .UNSPECIFIED., .F., .F.,
 ( 4, 4 ),
 ( 0.6192157509887148414, 0.6202164980294804231 ),
 .UNSPECIFIED. ) ;
#48282=DIRECTION ( 'NONE',  ( 3.773278334444166432E-23, -1.000000000000000000, 0.000000000000000000 ) ) ;
#48283=CARTESIAN_POINT ( 'NONE',  ( 1.468936567494551593, -19.95401460376903913, -1.500000000000002220 ) ) ;
#48284=DIRECTION ( 'NONE',  ( 0.000000000000000000, 0.9999999999976377785, 2.173523156925979128E-06 ) ) ;
#48286=ORIENTED_EDGE ( 'NONE', *, *, #10026, .T. ) ;
#48289=DIRECTION ( 'NONE',  ( 0.000000000000000000, -2.173523156925980399E-06, 0.9999999999976378895 ) ) ;
#48290=FACE_OUTER_BOUND ( 'NONE', #24181, .T. ) ;
#48291=CARTESIAN_POINT ( 'NONE',  ( -117.7765869487822812, -25.31326647857923362, 3.500947721614712016 ) ) ;
#48292=CARTESIAN_POINT ( 'NONE',  ( -83.59538777415443178, -23.96119346886880308, -0.6495511937832110227 ) ) ;
#48294=CARTESIAN_POINT ( 'NONE',  ( -100.9392423175550988, -25.11539320716599732, 2.804431449967498491 ) ) ;
#48296=B_SPLINE_CURVE_WITH_KNOTS ( 'NONE', 3,
 ( #46782, #40174, #10221, #87336 ),
 .UNSPECIFIED., .F., .F.,
 ( 4, 4 ),
 ( 0.000000000000000000, 9.999999999998897304E-05 ),
 .UNSPECIFIED. ) ;
#48297=CARTESIAN_POINT ( 'NONE',  ( 16.58868386459195676, 11.68684615565071283, -1.500000000000002220 ) ) ;
#48298=ADVANCED_FACE ( 'NONE', ( #98980 ), #22843, .F. ) ;
#48299=EDGE_CURVE ( 'NONE', #42265, #98447, #59244, .T. ) ;
#48300=PLANE ( 'NONE',  #32312 ) ;
#48301=CARTESIAN_POINT ( 'NONE',  ( -34.62287095715005592, -24.64898659630367206, 1.056161002820817485 ) ) ;
#48302=FACE_OUTER_BOUND ( 'NONE', #77148, .T. ) ;
#48305=B_SPLINE_CURVE_WITH_KNOTS ( 'NONE', 3,
 ( #24428, #8716, #47782, #25935 ),
 .UNSPECIFIED., .F., .F.,
 ( 4, 4 ),
 ( 0.000000000000000000, 9.999999999998897304E-05 ),
 .UNSPECIFIED. ) ;
#48306=CARTESIAN_POINT ( 'NONE',  ( -20.44436638909326120, 5.324712401148210539, 11.49999999999999645 ) ) ;
#48307=CARTESIAN_POINT ( 'NONE',  ( -9.153499762860807465, 20.15527781828815534, -1.500000000000002220 ) ) ;
#48308=B_SPLINE_CURVE_WITH_KNOTS ( 'NONE', 3,
 ( #66947, #59322, #83138, #28361 ),
 .UNSPECIFIED., .F., .F.,
 ( 4, 4 ),
 ( 0.000000000000000000, 0.0001000000000000028644 ),
 .UNSPECIFIED. ) ;
#48310=CARTESIAN_POINT ( 'NONE',  ( 15.43701773751798001, -13.56989305476470875, 11.49999999999998934 ) ) ;
#48312=EDGE_LOOP ( 'NONE', ( #98526, #49196, #53839, #29707 ) ) ;
#48316=CARTESIAN_POINT ( 'NONE',  ( -54.64429893256247794, -23.96119346886879953, -0.6495511937832153526 ) ) ;
#48317=CARTESIAN_POINT ( 'NONE',  ( -70.52287095715007581, -24.91570333825474748, 8.075032458260896107 ) ) ;
#48318=ORIENTED_EDGE ( 'NONE', *, *, #43655, .F. ) ;
#48319=ORIENTED_EDGE ( 'NONE', *, *, #71223, .T. ) ;
#48321=FACE_OUTER_BOUND ( 'NONE', #69568, .T. ) ;
#48322=CARTESIAN_POINT ( 'NONE',  ( -29.52287095715006515, -23.38906523657919578, -1.443836447538998424 ) ) ;
#48324=CARTESIAN_POINT ( 'NONE',  ( 4.906390264955167169, 20.09725327650800608, -1.500000000000002220 ) ) ;
#48326=CARTESIAN_POINT ( 'NONE',  ( -19.97641003480726241, 8.421946895145676848, 11.49999999999999645 ) ) ;
#48329=LINE ( 'NONE', #63061, #12410 ) ;
#48330=CARTESIAN_POINT ( 'NONE',  ( 1.926536275058113867, -22.33200895297504474, -1.500000000000002220 ) ) ;
#48331=VECTOR ( 'NONE', #49901, 1000.000000000000114 ) ;
#48333=CARTESIAN_POINT ( 'NONE',  ( -47.56045540262851290, -23.73791477778911485, 11.05961554403170766 ) ) ;
#48335=VERTEX_POINT ( 'NONE', #53332 ) ;
#48336=CARTESIAN_POINT ( 'NONE',  ( -38.62287095715005592, -23.47593901973091235, -1.443836447539011525 ) ) ;
#48337=CARTESIAN_POINT ( 'NONE',  ( -76.62287095715007013, -24.64965695001468404, 8.947790433994182280 ) ) ;
#48340=CARTESIAN_POINT ( 'NONE',  ( -71.52287095715007581, -23.47596703998600631, 11.44779298504228748 ) ) ;
#48343=CARTESIAN_POINT ( 'NONE',  ( -108.5228709571500758, -23.47593901973090524, -1.443836447538996204 ) ) ;
#48344=CARTESIAN_POINT ( 'NONE',  ( -10.85727797829764185, 18.24708236899833835, -1.500000000000002220 ) ) ;
#48346=CARTESIAN_POINT ( 'NONE',  ( -50.48000260994784583, -24.83618233451449697, 1.606449574219540599 ) ) ;
#48347=CARTESIAN_POINT ( 'NONE',  ( -8.041798833237560729, -20.28069125152608976, 11.49999999999998934 ) ) ;
#48348=CARTESIAN_POINT ( 'NONE',  ( -103.6358334257766955, -23.48786465467241413, 11.44779295918254292 ) ) ;
#48350=DIRECTION ( 'NONE',  ( -0.000000000000000000, 2.173523156925979552E-06, -0.9999999999976378895 ) ) ;
#48351=CARTESIAN_POINT ( 'NONE',  ( -60.62287095715004881, -29.50249982740957577, 7.747779886224967605 ) ) ;
#48352=CARTESIAN_POINT ( 'NONE',  ( 16.27406392464308027, 14.57352745747340172, -1.500000000000002220 ) ) ;
#48353=CARTESIAN_POINT ( 'NONE',  ( -30.57287095715004810, -25.30498646304936727, 4.433167295270071584 ) ) ;
#48354=ORIENTED_EDGE ( 'NONE', *, *, #42594, .T. ) ;
#48355=CARTESIAN_POINT ( 'NONE',  ( -65.62287095715005592, -25.00158670708909270, 2.256160236439166855 ) ) ;
#48357=ORIENTED_EDGE ( 'NONE', *, *, #48818, .T. ) ;
#48358=ORIENTED_EDGE ( 'NONE', *, *, #28124, .F. ) ;
#48362=CARTESIAN_POINT ( 'NONE',  ( -113.6228709571500417, -23.48783264082479150, -1.443836473390060160 ) ) ;
#48363=CARTESIAN_POINT ( 'NONE',  ( -1.624102159174229731, 21.17438964843747584, -1.500000000000002220 ) ) ;
#48364=PLANE ( 'NONE',  #72544 ) ;
#48365=CARTESIAN_POINT ( 'NONE',  ( -41.26959558397305727, -25.07899898050004950, 7.338714981574760543 ) ) ;
#48366=CARTESIAN_POINT ( 'NONE',  ( -33.62287095715005592, -24.65952944569304250, 1.056160979905690356 ) ) ;
#48368=CARTESIAN_POINT ( 'NONE',  ( 4.481524277812761525, 18.85844072219565604, 11.49999999999998934 ) ) ;
#48369=EDGE_CURVE ( 'NONE', #53220, #56586, #42375, .T. ) ;
#48370=EDGE_CURVE ( 'NONE', #21744, #55188, #64118, .T. ) ;
#48371=CARTESIAN_POINT ( 'NONE',  ( -45.53831601786538386, -24.52300882791528380, 0.6510814631126234930 ) ) ;
#48372=VERTEX_POINT ( 'NONE', #14745 ) ;
#48373=CARTESIAN_POINT ( 'NONE',  ( 8.918240691521024388, 17.32521578647535776, 11.49999999999999645 ) ) ;
#48374=CARTESIAN_POINT ( 'NONE',  ( -99.64934318012689118, -25.31535474791540707, 4.927356294767410105 ) ) ;
#48380=FACE_OUTER_BOUND ( 'NONE', #57294, .T. ) ;
#48381=CARTESIAN_POINT ( 'NONE',  ( -19.15281226579456231, 4.489446101945751444, -1.500000000000002220 ) ) ;
#48382=ORIENTED_EDGE ( 'NONE', *, *, #46743, .F. ) ;
#48383=FACE_OUTER_BOUND ( 'NONE', #51680, .T. ) ;
#48384=CARTESIAN_POINT ( 'NONE',  ( 15.98122378838116120, 16.67787885001082770, -1.500000000000002220 ) ) ;
#48387=PLANE ( 'NONE',  #92063 ) ;
#48388=DIRECTION ( 'NONE',  ( -3.773278334444167608E-23, 1.000000000000000000, 0.000000000000000000 ) ) ;
#48389=CARTESIAN_POINT ( 'NONE',  ( -92.62287095715008434, -24.34917612406837861, 0.1852690917426660921 ) ) ;
#48390=CARTESIAN_POINT ( 'NONE',  ( -97.62356141978688129, -24.66019654487199730, 8.947790411086115725 ) ) ;
#48391=CARTESIAN_POINT ( 'NONE',  ( -78.92688763707079147, -25.20144873054373136, 6.835696071488102099 ) ) ;
#48392=DIRECTION ( 'NONE',  ( -3.773278334453080206E-23, 0.9999999999976377785, 2.173523156925979552E-06 ) ) ;
#48393=EDGE_CURVE ( 'NONE', #26377, #81873, #13209, .T. ) ;
#48394=CARTESIAN_POINT ( 'NONE',  ( -129.5896973008811983, -24.34968618360934656, 0.1864209137778921610 ) ) ;
#48395=CARTESIAN_POINT ( 'NONE',  ( -99.12380231474227799, -25.26400682238891093, 4.001575156371126596 ) ) ;
#48396=CARTESIAN_POINT ( 'NONE',  ( -11.57717615966994273, 16.22069937712612031, 11.49999999999998934 ) ) ;
#48397=B_SPLINE_CURVE_WITH_KNOTS ( 'NONE', 3,
 ( #95164, #9922, #26149, #25648, #87045, #17536 ),
 .UNSPECIFIED., .F., .F.,
 ( 4, 2, 4 ),
 ( 0.000000000000000000, 0.001380901958385387027, 0.002761803916770774053 ),
 .UNSPECIFIED. ) ;
#48398=CARTESIAN_POINT ( 'NONE',  ( -100.4856528238762081, -25.19529134689449634, 3.295791984263175767 ) ) ;
#48399=EDGE_CURVE ( 'NONE', #84073, #33754, #18081, .T. ) ;
#48400=CARTESIAN_POINT ( 'NONE',  ( 19.67252036444665109, 2.607452956813616218, -1.500000000000002220 ) ) ;
#48401=ORIENTED_EDGE ( 'NONE', *, *, #91063, .F. ) ;
#48404=CARTESIAN_POINT ( 'NONE',  ( -71.52287095715006160, -23.94994826722565406, -0.6494450866342743600 ) ) ;
#48407=CARTESIAN_POINT ( 'NONE',  ( -51.52469858490392340, -25.25107916704070732, 6.255584458614488419 ) ) ;
#48408=CARTESIAN_POINT ( 'NONE',  ( -116.5228709571500332, -24.66019654487200086, 8.947790411086113949 ) ) ;
#48409=CARTESIAN_POINT ( 'NONE',  ( -20.73834036848188234, 1.213307192923735345, 11.49999999999999645 ) ) ;
#48410=CARTESIAN_POINT ( 'NONE',  ( -102.2228709571500502, -23.47596703998600276, 11.44779298504227683 ) ) ;
#48411=CARTESIAN_POINT ( 'NONE',  ( -40.55620429048340014, -24.99132157543166244, 2.256160258750668390 ) ) ;
#48412=CARTESIAN_POINT ( 'NONE',  ( 22.73759373355791169, -1.750760473330008171, 11.49999999999999645 ) ) ;
#48414=CARTESIAN_POINT ( 'NONE',  ( -69.49773674714293747, -24.51314013834315375, 0.6176544820404143987 ) ) ;
#48415=PLANE ( 'NONE',  #64659 ) ;
#48416=ORIENTED_EDGE ( 'NONE', *, *, #44083, .T. ) ;
#48417=AXIS2_PLACEMENT_3D ( 'NONE', #94075, #92569, #7333 ) ;
#48418=CARTESIAN_POINT ( 'NONE',  ( -6.636546740042271963, -19.09123619949631134, -1.500000000000002220 ) ) ;
#48419=EDGE_CURVE ( 'NONE', #23708, #26794, #56923, .T. ) ;
#48421=CARTESIAN_POINT ( 'NONE',  ( -90.22287095715005023, -23.47596703998600631, 11.44779298504227860 ) ) ;
#48422=CARTESIAN_POINT ( 'NONE',  ( -110.5228709571500048, -24.52323809116983355, 9.355190652339414825 ) ) ;
#48424=DIRECTION ( 'NONE',  ( -3.773278334453079618E-23, 0.9999999999976377785, 2.173523156925978705E-06 ) ) ;
#48426=CARTESIAN_POINT ( 'NONE',  ( 16.79232260237064978, 10.84791536263152523, -1.500000000000002220 ) ) ;
#48427=CARTESIAN_POINT ( 'NONE',  ( -32.62287095715004881, -24.65952944569304250, 1.056160979905691688 ) ) ;
#48428=CARTESIAN_POINT ( 'NONE',  ( -7.180602670292889123, -19.69607742855361465, 11.49999999999999645 ) ) ;
#48430=CARTESIAN_POINT ( 'NONE',  ( -52.52287095715006870, -24.64965694238574656, 8.947790433994203596 ) ) ;
#48431=CARTESIAN_POINT ( 'NONE',  ( -10.28628152547328511, -19.52461415289770130, -1.500000000000002220 ) ) ;
#48434=VECTOR ( 'NONE', #40401, 1000.000000000000114 ) ;
#48436=CARTESIAN_POINT ( 'NONE',  ( -127.5895376238166961, -23.48786465467242124, 11.44779295918253403 ) ) ;
#48437=CARTESIAN_POINT ( 'NONE',  ( -49.51045894826389571, -25.27344895790480450, 3.920634769891420568 ) ) ;
#48445=CARTESIAN_POINT ( 'NONE',  ( -101.2911250451791858, -25.10935867328099391, 3.130826437452274735 ) ) ;
#48446=CARTESIAN_POINT ( 'NONE',  ( -94.62287095715005592, -24.64965695001469115, 8.947790433994180503 ) ) ;
#48447=CARTESIAN_POINT ( 'NONE',  ( 19.85418835109896563, -5.301297255791479479, -1.500000000000002220 ) ) ;
#48449=VERTEX_POINT ( 'NONE', #12638 ) ;
#48450=CARTESIAN_POINT ( 'NONE',  ( -99.30778403274287314, -25.26531023543898158, 5.994093549950689770 ) ) ;
#48453=CARTESIAN_POINT ( 'NONE',  ( 16.98343680692684643, -14.46476453587665389, -1.500000000000002220 ) ) ;
#48454=EDGE_CURVE ( 'NONE', #90958, #40108, #70202, .T. ) ;
#48456=CARTESIAN_POINT ( 'NONE',  ( -0.02086824871851766100, -22.77984412121519497, 2.712351064733621531 ) ) ;
#48458=ORIENTED_EDGE ( 'NONE', *, *, #84409, .F. ) ;
#48462=CARTESIAN_POINT ( 'NONE',  ( -2.238888094254589234, -20.74146561784671761, 11.49999999999998934 ) ) ;
#48463=ORIENTED_EDGE ( 'NONE', *, *, #40504, .T. ) ;
#48464=CARTESIAN_POINT ( 'NONE',  ( -79.52287095715004739, -23.73934037231757088, 11.05740245334329508 ) ) ;
#48467=CARTESIAN_POINT ( 'NONE',  ( -68.94461706535129508, -25.25935091778287855, 6.371760082740177467 ) ) ;
#48469=CARTESIAN_POINT ( 'NONE',  ( 2.841100885065937387, 20.89556961663114265, -1.500000000000002220 ) ) ;
#48470=ORIENTED_EDGE ( 'NONE', *, *, #18311, .T. ) ;
#48473=LINE ( 'NONE', #79401, #36865 ) ;
#48474=CARTESIAN_POINT ( 'NONE',  ( -105.6228709571500275, -25.00182538069145721, 7.747789668545099317 ) ) ;
#48476=CARTESIAN_POINT ( 'NONE',  ( -86.58557003059961232, -24.51419770103155926, 9.386484678747176957 ) ) ;
#48477=B_SPLINE_CURVE_WITH_KNOTS ( 'NONE', 3,
 ( #31724, #25098, #64708, #80398, #41341, #8886 ),
 .UNSPECIFIED., .F., .F.,
 ( 4, 2, 4 ),
 ( 6.384118678610730862E-06, 0.001386860460828374334, 0.002767336802978137989 ),
 .UNSPECIFIED. ) ;
#48478=CARTESIAN_POINT ( 'NONE',  ( -59.52207695799008746, -23.48783264082476308, -1.443836473390097908 ) ) ;
#48479=CARTESIAN_POINT ( 'NONE',  ( -108.9573283046188408, -25.29252521095624928, 4.249509941946580938 ) ) ;
#48481=CARTESIAN_POINT ( 'NONE',  ( -14.74362065938029076, 16.57599527146691898, 11.49999999999999645 ) ) ;
#48482=ORIENTED_EDGE ( 'NONE', *, *, #10309, .F. ) ;
#48483=CARTESIAN_POINT ( 'NONE',  ( -99.07695620119221758, -25.30872027043050210, 5.427344019169676237 ) ) ;
#48484=PLANE ( 'NONE',  #73209 ) ;
#48485=ORIENTED_EDGE ( 'NONE', *, *, #77638, .T. ) ;
#48486=CARTESIAN_POINT ( 'NONE',  ( 20.48348528492645571, -9.684159049092739835, 11.49999999999998934 ) ) ;
#48487=VECTOR ( 'NONE', #63187, 1000.000000000000114 ) ;
#48489=VERTEX_POINT ( 'NONE', #11144 ) ;
#48490=EDGE_LOOP ( 'NONE', ( #95627, #38833, #99442, #58105 ) ) ;
#48493=CARTESIAN_POINT ( 'NONE',  ( 20.11291949428234105, -1.170665973999911902, 11.49999999999998934 ) ) ;
#48495=ORIENTED_EDGE ( 'NONE', *, *, #61337, .F. ) ;
#48497=CARTESIAN_POINT ( 'NONE',  ( -130.5728709571500872, -25.40555871708352953, 4.425364043583297935 ) ) ;
#48498=CARTESIAN_POINT ( 'NONE',  ( 3.152853332073482839, 22.16862046936333286, -1.500000000000002220 ) ) ;
#48499=ORIENTED_EDGE ( 'NONE', *, *, #97413, .F. ) ;
#48500=ORIENTED_EDGE ( 'NONE', *, *, #69956, .F. ) ;
#48501=CARTESIAN_POINT ( 'NONE',  ( -89.40841769935769889, -25.13785473458444031, 7.104038777038262253 ) ) ;
#48502=CARTESIAN_POINT ( 'NONE',  ( -48.52287095715006160, -24.66019654487200086, 8.947790411086119278 ) ) ;
#48503=CARTESIAN_POINT ( 'NONE',  ( -96.52287095715006160, -23.47596703998600631, 11.44779298504228215 ) ) ;
#48505=CARTESIAN_POINT ( 'NONE',  ( -30.63241211973601352, -23.78062553189671746, -0.9709657327914300584 ) ) ;
#48506=CARTESIAN_POINT ( 'NONE',  ( -13.92019785312828972, -13.74635529968554515, 11.49999999999998934 ) ) ;
#48509=CARTESIAN_POINT ( 'NONE',  ( 20.90071823198991297, 5.034746273075951351, 11.49999999999998934 ) ) ;
#48510=CARTESIAN_POINT ( 'NONE',  ( -36.52287095715006870, -23.47593901973090169, -1.443836447538997314 ) ) ;
#48511=B_SPLINE_CURVE_WITH_KNOTS ( 'NONE', 3,
 ( #61445, #38592, #31982, #78132, #70544, #22344 ),
 .UNSPECIFIED., .F., .F.,
 ( 4, 2, 4 ),
 ( 6.384118678611516061E-06, 0.001386860460828373250, 0.002767336802978134953 ),
 .UNSPECIFIED. ) ;
#48514=CARTESIAN_POINT ( 'NONE',  ( -80.62287095715005592, -24.99156045073393173, 7.747789690856161648 ) ) ;
#48515=CARTESIAN_POINT ( 'NONE',  ( -22.92702450682246251, 0.3551139841105944162, -1.500000000000002220 ) ) ;
#48521=CARTESIAN_POINT ( 'NONE',  ( 1.236116150138429903, -20.07036509671028668, 11.49999999999999645 ) ) ;
#48522=LINE ( 'NONE', #3847, #83530 ) ;
#48524=EDGE_CURVE ( 'NONE', #26860, #15801, #65388, .T. ) ;
#48525=EDGE_CURVE ( 'NONE', #62936, #39701, #1198, .T. ) ;
#48526=CARTESIAN_POINT ( 'NONE',  ( -121.6228709571500417, -24.50321055353806798, 9.387540953477529371 ) ) ;
#48527=DIRECTION ( 'NONE',  ( -3.773278334453079618E-23, 0.9999999999976377785, 2.173523156925979975E-06 ) ) ;
#48528=CARTESIAN_POINT ( 'NONE',  ( -49.62287095715005592, -24.66019654487199020, 8.947790411086135265 ) ) ;
#48529=CARTESIAN_POINT ( 'NONE',  ( -19.53060160647804722, 3.385818350044136338, -1.500000000000002220 ) ) ;
#48531=CARTESIAN_POINT ( 'NONE',  ( 0.2638585030419089428, -21.76204025362994798, -1.500000000000002220 ) ) ;
#48533=CARTESIAN_POINT ( 'NONE',  ( 5.117700956428186565, 18.95590836763280862, -1.500000000000002220 ) ) ;
#48536=EDGE_CURVE ( 'NONE', #2820, #41820, #63932, .T. ) ;
#48540=CARTESIAN_POINT ( 'NONE',  ( -103.5228709571500616, -24.50216790748205042, 0.6166512839542598323 ) ) ;
#48541=CARTESIAN_POINT ( 'NONE',  ( -54.62287095715005592, -29.50247984919015209, -1.443849546365058689 ) ) ;
#48542=CARTESIAN_POINT ( 'NONE',  ( 16.43461662053371697, -12.34185696772103391, 11.49999999999999645 ) ) ;
#48545=CARTESIAN_POINT ( 'NONE',  ( -11.86362535333686807, -19.25999739251378173, 11.49999999999999645 ) ) ;
#48546=VERTEX_POINT ( 'NONE', #12134 ) ;
#48547=CARTESIAN_POINT ( 'NONE',  ( -69.86129607977629519, -25.25639579666412615, 7.001236270658951710 ) ) ;
#48548=CARTESIAN_POINT ( 'NONE',  ( -98.62287095715005592, -23.47593901973091235, -1.443836447539001089 ) ) ;
#48549=CARTESIAN_POINT ( 'NONE',  ( -97.55239856924187336, -24.15543982623907837, -0.2315651400026600415 ) ) ;
#48550=CARTESIAN_POINT ( 'NONE',  ( -26.43215695177226010, -24.84863243741908434, 3.116149861069652083 ) ) ;
#48553=CARTESIAN_POINT ( 'NONE',  ( -110.5228709571500474, -24.63287334234179582, 0.9662140553045319713 ) ) ;
#48556=VERTEX_POINT ( 'NONE', #10650 ) ;
#48557=EDGE_CURVE ( 'NONE', #55957, #39695, #23990, .T. ) ;
#48558=CARTESIAN_POINT ( 'NONE',  ( -79.46066275308743343, -25.31596331910725084, 5.472043507825191888 ) ) ;
#48559=CARTESIAN_POINT ( 'NONE',  ( -18.62658236799572720, 13.20813282334384553, 11.49999999999998934 ) ) ;
#48560=CARTESIAN_POINT ( 'NONE',  ( -110.6052975838258590, -25.18890164017962974, 3.322127376059897053 ) ) ;
#48562=CARTESIAN_POINT ( 'NONE',  ( -106.6228709571500559, -23.73934037231757799, 11.05740245334328442 ) ) ;
#48564=CARTESIAN_POINT ( 'NONE',  ( 22.48772827135616126, 0.8316936486096353498, 11.49999999999999645 ) ) ;
#48565=ORIENTED_EDGE ( 'NONE', *, *, #37071, .T. ) ;
#48568=CARTESIAN_POINT ( 'NONE',  ( -20.77788740438921522, -7.151594987469691134, 11.49999999999998934 ) ) ;
#48569=CARTESIAN_POINT ( 'NONE',  ( -114.5228709571500616, -23.95044443724992789, 10.65354141964649592 ) ) ;
#48570=VECTOR ( 'NONE', #45973, 1000.000000000000114 ) ;
#48572=CARTESIAN_POINT ( 'NONE',  ( -69.27702271707670434, -25.12257852196836438, 7.104949132215303997 ) ) ;
#48573=ORIENTED_EDGE ( 'NONE', *, *, #16028, .T. ) ;
#48574=PLANE ( 'NONE',  #31417 ) ;
#48575=CARTESIAN_POINT ( 'NONE',  ( -71.52287095715007581, -29.50250243563736774, 8.947779886222143375 ) ) ;
#48576=ORIENTED_EDGE ( 'NONE', *, *, #37112, .F. ) ;
#48577=CARTESIAN_POINT ( 'NONE',  ( -15.16157141410761966, -13.82251119679066953, 11.49999999999998934 ) ) ;
#48580=VERTEX_POINT ( 'NONE', #64968 ) ;
#48581=ORIENTED_EDGE ( 'NONE', *, *, #49791, .T. ) ;
#48583=CARTESIAN_POINT ( 'NONE',  ( 22.95697726795019378, -2.620641032420567118, 11.49999999999998934 ) ) ;
#48585=CARTESIAN_POINT ( 'NONE',  ( 0.8761431260907562857, 20.31601184897261092, -1.500000000000002220 ) ) ;
#48586=ORIENTED_EDGE ( 'NONE', *, *, #97536, .F. ) ;
#48588=CARTESIAN_POINT ( 'NONE',  ( -51.52287095715006870, -23.47596703998600631, 11.44779298504229104 ) ) ;
#48589=EDGE_CURVE ( 'NONE', #40340, #88666, #1003, .T. ) ;
#48590=CARTESIAN_POINT ( 'NONE',  ( -114.6228709571500843, -24.35013146730204525, 9.818937971375108376 ) ) ;
#48592=CARTESIAN_POINT ( 'NONE',  ( -19.33005188562793819, 9.364626179424670127, 11.49999999999999645 ) ) ;
#48593=ORIENTED_EDGE ( 'NONE', *, *, #21109, .F. ) ;
#48594=CARTESIAN_POINT ( 'NONE',  ( -75.53786830476269643, -24.83618233451450763, 1.606449574219540599 ) ) ;
#48596=ORIENTED_EDGE ( 'NONE', *, *, #79038, .T. ) ;
#48597=CARTESIAN_POINT ( 'NONE',  ( -15.27568272636907665, 14.01247568063241999, -1.500000000000002220 ) ) ;
#48600=CARTESIAN_POINT ( 'NONE',  ( -91.62287095715004170, -24.64898659630368627, 1.056161002820827921 ) ) ;
#48602=FACE_OUTER_BOUND ( 'NONE', #44363, .T. ) ;
#48604=ORIENTED_EDGE ( 'NONE', *, *, #78181, .T. ) ;
#48605=ORIENTED_EDGE ( 'NONE', *, *, #16772, .T. ) ;
#48608=CARTESIAN_POINT ( 'NONE',  ( -29.68527933152038045, -25.15099025512602537, 3.470668543855588428 ) ) ;
#48609=CARTESIAN_POINT ( 'NONE',  ( 21.99661117994144988, 0.4758108284031232760, 11.49999999999999645 ) ) ;
#48612=CARTESIAN_POINT ( 'NONE',  ( 14.59886444729927923, 17.24780449347180067, -1.500000000000002220 ) ) ;
#48613=CARTESIAN_POINT ( 'NONE',  ( 12.56776941831905070, -16.83212535568997126, 11.49999999999998934 ) ) ;
#48614=CARTESIAN_POINT ( 'NONE',  ( -62.52287095715006160, -24.50216790748204687, 0.6166512839542488411 ) ) ;
#48616=ORIENTED_EDGE ( 'NONE', *, *, #45545, .T. ) ;
#48619=DIRECTION ( 'NONE',  ( 0.000000000000000000, 0.9999999999976377785, 2.173523156925979128E-06 ) ) ;
#48620=ORIENTED_EDGE ( 'NONE', *, *, #96308, .T. ) ;
#48621=CARTESIAN_POINT ( 'NONE',  ( 10.59196434753715010, 18.29633683537252509, -1.500000000000002220 ) ) ;
#48623=CARTESIAN_POINT ( 'NONE',  ( -50.58702570880215177, -25.03148741087247942, 7.558809112751002424 ) ) ;
#48624=VECTOR ( 'NONE', #99572, 1000.000000000000114 ) ;
#48625=CARTESIAN_POINT ( 'NONE',  ( -71.20541289166536103, -25.31502801509702749, 4.885889949323629189 ) ) ;
#48626=DIRECTION ( 'NONE',  ( -3.773278334453079030E-23, 0.9999999999976377785, 2.173523156925979128E-06 ) ) ;
#48627=CARTESIAN_POINT ( 'NONE',  ( 14.71430157977438924, -16.63553917435140406, -1.500000000000002220 ) ) ;
#48628=CARTESIAN_POINT ( 'NONE',  ( -114.6254336291504501, -24.34968618360934656, 0.1864209137778972403 ) ) ;
#48629=ORIENTED_EDGE ( 'NONE', *, *, #88086, .F. ) ;
#48630=CARTESIAN_POINT ( 'NONE',  ( -117.5228709571500758, -29.50247984919015209, -1.443849546365046699 ) ) ;
#48631=DIRECTION ( 'NONE',  ( -3.773278334453079030E-23, 0.9999999999976377785, 2.173523156925979128E-06 ) ) ;
#48632=CARTESIAN_POINT ( 'NONE',  ( -10.03281922573575002, -16.61734169602722488, 11.49999999999999645 ) ) ;
#48633=VECTOR ( 'NONE', #94132, 1000.000000000000114 ) ;
#48634=CARTESIAN_POINT ( 'NONE',  ( -36.53263999733187006, -24.51419770103156637, 9.386484678747175181 ) ) ;
#48635=CARTESIAN_POINT ( 'NONE',  ( -82.62287095715005592, -23.47593901973091235, -1.443836447539004642 ) ) ;
#48636=VECTOR ( 'NONE', #96478, 1000.000000000000114 ) ;
#48637=CARTESIAN_POINT ( 'NONE',  ( 13.74000504945409418, 13.82049530813991467, -1.500000000000002220 ) ) ;
#48639=CARTESIAN_POINT ( 'NONE',  ( -21.42254595866439004, -0.3319015934494286557, 11.49999999999998934 ) ) ;
#48641=CARTESIAN_POINT ( 'NONE',  ( -60.64002619184125109, -24.40133493613623372, 9.663955038888268234 ) ) ;
#48642=CARTESIAN_POINT ( 'NONE',  ( -51.50748557923905224, -23.96119346886880663, -0.6495511937832119109 ) ) ;
#48643=DIRECTION ( 'NONE',  ( 0.000000000000000000, -0.9999999999976377785, -2.173523156925979128E-06 ) ) ;
#48644=CARTESIAN_POINT ( 'NONE',  ( -22.52399778787742335, 3.408274809117095572, -1.500000000000002220 ) ) ;
#48648=CARTESIAN_POINT ( 'NONE',  ( -106.6248927510747819, -24.51419770103158768, 9.386484678747164523 ) ) ;
#48649=DIRECTION ( 'NONE',  ( -1.000000000000000000, -3.773278334444167608E-23, -8.201307833595939069E-29 ) ) ;
#48650=CARTESIAN_POINT ( 'NONE',  ( 10.41257876278241845, -16.90412932818451353, 11.49999999999999645 ) ) ;
#48654=CARTESIAN_POINT ( 'NONE',  ( -92.52287095715006160, -23.48786465467241769, 11.44779295918254292 ) ) ;
#48656=DIRECTION ( 'NONE',  ( 3.773278334444167608E-23, -1.000000000000000000, 0.000000000000000000 ) ) ;
#48659=CARTESIAN_POINT ( 'NONE',  ( -51.32120688873476411, -25.10935831503348581, 3.174475921786763077 ) ) ;
#48660=CARTESIAN_POINT ( 'NONE',  ( 4.495418090846292181, 21.21921847905042569, 11.49999999999998934 ) ) ;
#48661=PLANE ( 'NONE',  #86844 ) ;
#48662=CARTESIAN_POINT ( 'NONE',  ( -17.65537929698502495, 8.214918384300796461, -1.500000000000002220 ) ) ;
#48665=ORIENTED_EDGE ( 'NONE', *, *, #59641, .F. ) ;
#48667=CARTESIAN_POINT ( 'NONE',  ( 18.38310620586021571, 8.829655622120887060, 11.49999999999999645 ) ) ;
#48673=CARTESIAN_POINT ( 'NONE',  ( -29.62287095715003815, -23.88347863494311341, -0.6494985534383576065 ) ) ;
#48674=CARTESIAN_POINT ( 'NONE',  ( -48.92287095715006018, -23.47596703998600276, 11.44779298504227683 ) ) ;
#48676=CARTESIAN_POINT ( 'NONE',  ( -38.62287095715005592, -23.47596703998600276, 11.44779298504227505 ) ) ;
#48677=CARTESIAN_POINT ( 'NONE',  ( -106.5228709571500758, -29.50250243563736774, 8.947779886222136270 ) ) ;
#48678=ORIENTED_EDGE ( 'NONE', *, *, #3128, .F. ) ;
#48679=CARTESIAN_POINT ( 'NONE',  ( -66.49650470888528275, -24.51419770103157347, 9.386484678747176957 ) ) ;
#48680=CARTESIAN_POINT ( 'NONE',  ( 20.74614131242519477, 9.816050768296040729, 11.49999999999999645 ) ) ;
#48681=CARTESIAN_POINT ( 'NONE',  ( 5.860688371469950475, 21.97560254587667217, 11.49999999999998934 ) ) ;
#48683=CARTESIAN_POINT ( 'NONE',  ( -110.5501817371814468, -24.73531770709095312, 8.716586749053508498 ) ) ;
#48686=CARTESIAN_POINT ( 'NONE',  ( -110.5570708675502516, -23.85016227208580020, -0.8807180028928306426 ) ) ;
#48688=CARTESIAN_POINT ( 'NONE',  ( -8.129759772327192380, 20.32010563749377141, -1.500000000000002220 ) ) ;
#48689=CARTESIAN_POINT ( 'NONE',  ( -69.60832130884770663, -23.48786465467240703, 11.44779295918255002 ) ) ;
#48694=CARTESIAN_POINT ( 'NONE',  ( 18.82465703714932204, -7.861812626244089053, 11.49999999999998934 ) ) ;
#48696=VERTEX_POINT ( 'NONE', #13625 ) ;
#48697=CARTESIAN_POINT ( 'NONE',  ( 18.48385363477634513, -13.70420857335572506, -1.500000000000002220 ) ) ;
#48699=ORIENTED_EDGE ( 'NONE', *, *, #83832, .F. ) ;
#48701=CARTESIAN_POINT ( 'NONE',  ( -125.6228709571500559, -23.47593901973091235, -1.443836447538995760 ) ) ;
#48702=AXIS2_PLACEMENT_3D ( 'NONE', #25745, #80528, #33856 ) ;
#48703=CARTESIAN_POINT ( 'NONE',  ( -95.51303906205738770, -24.15503026093913874, -0.2815557561904519224 ) ) ;
#48705=CARTESIAN_POINT ( 'NONE',  ( 6.557060941508195739, 20.25493142521265355, 11.49999999999999645 ) ) ;
#48706=EDGE_LOOP ( 'NONE', ( #65573, #15844, #96982, #84193 ) ) ;
#48707=VECTOR ( 'NONE', #35949, 1000.000000000000114 ) ;
#48708=EDGE_LOOP ( 'NONE', ( #82732, #91239, #43381, #98982 ) ) ;
#48709=CARTESIAN_POINT ( 'NONE',  ( -7.359855604737914447, 20.98419016808480109, 11.49999999999998934 ) ) ;
#48710=CARTESIAN_POINT ( 'NONE',  ( 6.115004186001010922, -19.73231167505474559, -1.500000000000002220 ) ) ;
#48711=ADVANCED_FACE ( 'NONE', ( #60338 ), #28869, .T. ) ;
#48713=ORIENTED_EDGE ( 'NONE', *, *, #80476, .F. ) ;
#48715=EDGE_CURVE ( 'NONE', #99009, #46879, #56742, .T. ) ;
#48716=CARTESIAN_POINT ( 'NONE',  ( -95.62584158020946745, -24.83644354573579349, 8.397322867130096569 ) ) ;
#48717=ORIENTED_EDGE ( 'NONE', *, *, #79791, .T. ) ;
#48718=CARTESIAN_POINT ( 'NONE',  ( -95.52287095715003318, -24.14321612903117753, -0.2833117244520895750 ) ) ;
#48719=EDGE_LOOP ( 'NONE', ( #67992, #36183, #38556, #61713 ) ) ;
#48722=CARTESIAN_POINT ( 'NONE',  ( 20.33208665566141704, 4.825383418962623239, -1.500000000000002220 ) ) ;
#48723=CARTESIAN_POINT ( 'NONE',  ( -19.96805355746080934, -8.928269573510897672, 11.49999999999999645 ) ) ;
#48724=CARTESIAN_POINT ( 'NONE',  ( -73.63478229892059801, -24.15620529776628089, 10.23563542870660470 ) ) ;
#48726=CARTESIAN_POINT ( 'NONE',  ( -18.88510386880526326, 12.19974334031638641, -1.500000000000002220 ) ) ;
#48727=CARTESIAN_POINT ( 'NONE',  ( 5.579783289733251550, -20.15082174716252794, 11.49999999999998934 ) ) ;
#48728=CARTESIAN_POINT ( 'NONE',  ( -38.64173560969166488, -24.15543982623906771, -0.2315651400026570161 ) ) ;
#48729=CARTESIAN_POINT ( 'NONE',  ( -57.62287095715004881, -23.47593901973091235, -1.443836447539007972 ) ) ;
#48731=ORIENTED_EDGE ( 'NONE', *, *, #18778, .F. ) ;
#48733=ORIENTED_EDGE ( 'NONE', *, *, #13227, .F. ) ;
#48734=CARTESIAN_POINT ( 'NONE',  ( -52.56777431719391558, -23.48783264082478794, -1.443836473390069708 ) ) ;
#48735=ORIENTED_EDGE ( 'NONE', *, *, #57358, .T. ) ;
#48736=CARTESIAN_POINT ( 'NONE',  ( -21.12015818079280649, -3.594773940630530795, -1.500000000000002220 ) ) ;
#48737=CARTESIAN_POINT ( 'NONE',  ( -8.633843874998758494, 20.65557450359631630, 11.49999999999999645 ) ) ;
#48739=FACE_OUTER_BOUND ( 'NONE', #68302, .T. ) ;
#48740=CARTESIAN_POINT ( 'NONE',  ( 16.02493003730957000, -13.65669227992738577, 11.49999999999998934 ) ) ;
#48741=CARTESIAN_POINT ( 'NONE',  ( -30.48805280194831369, -24.57390550863043899, 9.174392229302920754 ) ) ;
#48742=CARTESIAN_POINT ( 'NONE',  ( -12.53609265798794681, -15.47265773855268378, -1.500000000000002220 ) ) ;
#48744=CARTESIAN_POINT ( 'NONE',  ( -80.84160375922890296, -25.29534361467446502, 4.579768035494214296 ) ) ;
#48745=CARTESIAN_POINT ( 'NONE',  ( 21.84380375219137349, -3.031640915038902762, -1.500000000000002220 ) ) ;
#48746=ORIENTED_EDGE ( 'NONE', *, *, #84471, .T. ) ;
#48747=CARTESIAN_POINT ( 'NONE',  ( -65.53456971742291159, -24.83644354573578994, 8.397322867130098345 ) ) ;
#48749=CARTESIAN_POINT ( 'NONE',  ( 20.57277012135545036, 3.371850554975475145, 11.49999999999999645 ) ) ;
#48750=CARTESIAN_POINT ( 'NONE',  ( -28.41196290477738273, -24.69444547851099614, 8.290116722409051064 ) ) ;
#48751=CARTESIAN_POINT ( 'NONE',  ( -27.51841088719901052, -24.59198966350803772, 1.634211142568063213 ) ) ;
#48753=CARTESIAN_POINT ( 'NONE',  ( 0.2649960030224881025, 21.33594185153759426, -1.500000000000002220 ) ) ;
#48759=CARTESIAN_POINT ( 'NONE',  ( -14.53490578827140212, -17.26895500059623956, -1.500000000000002220 ) ) ;
#48760=CARTESIAN_POINT ( 'NONE',  ( -68.62287095715005592, -29.50250243563736774, 8.947779886222143375 ) ) ;
#48761=EDGE_LOOP ( 'NONE', ( #98832, #79484, #33950, #73044 ) ) ;
#48764=CARTESIAN_POINT ( 'NONE',  ( 2.169241753049089727, -19.58708112974024829, 11.49999999999999645 ) ) ;
#48765=CARTESIAN_POINT ( 'NONE',  ( -32.07722060962683486, -25.28405270565852447, 3.734159825085341833 ) ) ;
#48767=ORIENTED_EDGE ( 'NONE', *, *, #56912, .F. ) ;
#48768=CARTESIAN_POINT ( 'NONE',  ( -111.5228709571500474, -24.50216790748206108, 0.6166512839542542812 ) ) ;
#48769=CARTESIAN_POINT ( 'NONE',  ( -99.52287095715009002, -24.66019654487200441, 8.947790411086119278 ) ) ;
#48771=CARTESIAN_POINT ( 'NONE',  ( -61.52287095715005449, -24.35013146730203815, 9.818937971375103047 ) ) ;
#48772=CARTESIAN_POINT ( 'NONE',  ( -97.62287095715005592, -29.50248528299804818, 1.056150453629042030 ) ) ;
#48773=CARTESIAN_POINT ( 'NONE',  ( -32.99388727629348494, -25.12026506542017046, 2.831122744435439209 ) ) ;
#48774=EDGE_CURVE ( 'NONE', #48827, #91131, #83298, .T. ) ;
#48775=DIRECTION ( 'NONE',  ( 0.000000000000000000, -2.173523156925979552E-06, 0.9999999999976378895 ) ) ;
#48776=CARTESIAN_POINT ( 'NONE',  ( 9.697495225759652726, 17.24774500829319734, 11.49999999999998934 ) ) ;
#48779=ADVANCED_FACE ( 'NONE', ( #97866 ), #6025, .T. ) ;
#48780=VECTOR ( 'NONE', #34598, 1000.000000000000114 ) ;
#48781=CARTESIAN_POINT ( 'NONE',  ( 15.40757771627215256, 13.04930689719894765, 11.49999999999999645 ) ) ;
#48787=CARTESIAN_POINT ( 'NONE',  ( -70.10882455230809285, -25.30100131183307610, 5.336495488474668036 ) ) ;
#48789=CARTESIAN_POINT ( 'NONE',  ( -122.5895376238167245, -23.47596703998600631, 11.44779298504227683 ) ) ;
#48790=B_SPLINE_CURVE_WITH_KNOTS ( 'NONE', 3,
 ( #65894, #35427, #2985, #66389, #58268, #49165 ),
 .UNSPECIFIED., .F., .F.,
 ( 4, 2, 4 ),
 ( 0.000000000000000000, 0.001380901958385383991, 0.002761803916770767982 ),
 .UNSPECIFIED. ) ;
#48791=CARTESIAN_POINT ( 'NONE',  ( -52.62287095715005592, -24.64898659630367561, 1.056161002820821038 ) ) ;
#48792=FACE_OUTER_BOUND ( 'NONE', #12216, .T. ) ;
#48793=CARTESIAN_POINT ( 'NONE',  ( 5.980626343040887249, -19.09133569553460319, 11.49999999999998934 ) ) ;
#48795=CARTESIAN_POINT ( 'NONE',  ( -57.62287095715004881, -24.66019654487199020, 8.947790411086131712 ) ) ;
#48797=CARTESIAN_POINT ( 'NONE',  ( -79.55873576538276382, -23.73791477778911840, 11.05961554403170943 ) ) ;
#48798=CARTESIAN_POINT ( 'NONE',  ( -35.48363359496615743, -24.52300882791529446, 0.6510814631126419227 ) ) ;
#48799=CARTESIAN_POINT ( 'NONE',  ( -79.48084051826894836, -25.29803721465439637, 5.434463432368143998 ) ) ;
#48801=B_SPLINE_CURVE_WITH_KNOTS ( 'NONE', 3,
 ( #84776, #77656, #85788, #92884 ),
 .UNSPECIFIED., .F., .F.,
 ( 4, 4 ),
 ( 0.000000000000000000, 9.999999999998897304E-05 ),
 .UNSPECIFIED. ) ;
#48802=CARTESIAN_POINT ( 'NONE',  ( -73.58797577400544299, -24.34968618360933590, 0.1864209137778805869 ) ) ;
#48804=CARTESIAN_POINT ( 'NONE',  ( -101.9682441342847596, -25.32724633150699844, 4.398074151685130495 ) ) ;
#48806=CARTESIAN_POINT ( 'NONE',  ( 14.61151973098085222, 14.07909450314327771, 11.49999999999998934 ) ) ;
#48809=CARTESIAN_POINT ( 'NONE',  ( -127.5554365995002541, -24.35071581493544102, 9.817618358456009275 ) ) ;
#48810=CARTESIAN_POINT ( 'NONE',  ( -59.57899832961151532, -24.66019654487199730, 8.947790411086124607 ) ) ;
#48813=CARTESIAN_POINT ( 'NONE',  ( -30.47287095715007510, -24.98308899733239130, 7.804029986632581739 ) ) ;
#48814=CARTESIAN_POINT ( 'NONE',  ( -17.67215177357914513, -11.65580189297658897, 11.49999999999999645 ) ) ;
#48815=B_SPLINE_CURVE_WITH_KNOTS ( 'NONE', 3,
 ( #56060, #17480, #40817, #33204 ),
 .UNSPECIFIED., .F., .F.,
 ( 4, 4 ),
 ( 0.4801287726817814461, 0.4891352039538970353 ),
 .UNSPECIFIED. ) ;
#48816=CARTESIAN_POINT ( 'NONE',  ( 21.13975321936677787, -6.629177502137091338, -1.500000000000002220 ) ) ;
#48818=EDGE_CURVE ( 'NONE', #43756, #63195, #42184, .T. ) ;
#48819=CARTESIAN_POINT ( 'NONE',  ( 7.805751503010069037, -19.01748540344778959, 11.49999999999998934 ) ) ;
#48820=ORIENTED_EDGE ( 'NONE', *, *, #52069, .T. ) ;
#48821=DIRECTION ( 'NONE',  ( 0.000000000000000000, -2.173523156925979552E-06, 0.9999999999976378895 ) ) ;
#48822=ORIENTED_EDGE ( 'NONE', *, *, #22368, .T. ) ;
#48823=CARTESIAN_POINT ( 'NONE',  ( -54.58256300931693517, -24.51314013834315020, 0.6176544820404069602 ) ) ;
#48824=CARTESIAN_POINT ( 'NONE',  ( -70.52287095715007581, -24.51254535375844412, 9.355368624242185405 ) ) ;
#48825=ORIENTED_EDGE ( 'NONE', *, *, #39586, .F. ) ;
#48827=VERTEX_POINT ( 'NONE', #72314 ) ;
#48828=CARTESIAN_POINT ( 'NONE',  ( -110.5097208737972778, -25.12185449762653278, 2.839826584255876973 ) ) ;
#48831=CARTESIAN_POINT ( 'NONE',  ( 20.27745880512110688, -4.159726151199424571, -1.500000000000002220 ) ) ;
#48832=CARTESIAN_POINT ( 'NONE',  ( 3.837509532605410278, -21.31939230324424628, 11.49999999999999645 ) ) ;
#48833=ORIENTED_EDGE ( 'NONE', *, *, #84216, .F. ) ;
#48834=CARTESIAN_POINT ( 'NONE',  ( -127.5895376238167245, -24.65952944569305316, 1.056160979905710118 ) ) ;
#48836=CARTESIAN_POINT ( 'NONE',  ( -4.914914792326205983, -21.87198836336805385, -1.500000000000002220 ) ) ;
#48837=CARTESIAN_POINT ( 'NONE',  ( -33.62287095715005592, -24.64965695001467694, 8.947790433994189385 ) ) ;
#48838=CARTESIAN_POINT ( 'NONE',  ( -71.62287095715007013, -24.51283580621364777, 0.6167428607019787012 ) ) ;
#48839=ORIENTED_EDGE ( 'NONE', *, *, #42707, .F. ) ;
#48840=CARTESIAN_POINT ( 'NONE',  ( -87.52287095715006160, -23.47596703998600631, 11.44779298504228393 ) ) ;
#48841=VECTOR ( 'NONE', #89807, 1000.000000000000114 ) ;
#48842=CARTESIAN_POINT ( 'NONE',  ( -120.6228709571500275, -24.52323809116984776, 9.355190652339421931 ) ) ;
#48844=ORIENTED_EDGE ( 'NONE', *, *, #22287, .F. ) ;
#48849=CARTESIAN_POINT ( 'NONE',  ( -94.62287095715005592, -24.64898659630528854, 1.056161002820827921 ) ) ;
#48850=CARTESIAN_POINT ( 'NONE',  ( 9.380127297304197143, -19.07726845333505494, -1.500000000000002220 ) ) ;
#48851=EDGE_LOOP ( 'NONE', ( #14747, #19824, #63101, #64307 ) ) ;
#48852=DIRECTION ( 'NONE',  ( 0.000000000000000000, 2.173523156925980399E-06, -0.9999999999976378895 ) ) ;
#48853=CARTESIAN_POINT ( 'NONE',  ( -15.20188179817220231, 15.67080601223297442, -1.500000000000002220 ) ) ;
#48854=CARTESIAN_POINT ( 'NONE',  ( -52.50765823405691890, -23.96169478059712787, 10.65365249895718769 ) ) ;
#48856=DIRECTION ( 'NONE',  ( -1.000000000000000000, -3.773278334444166432E-23, -8.201307841325785021E-29 ) ) ;
#48857=CARTESIAN_POINT ( 'NONE',  ( -12.54888962926113827, 17.92887824059606672, -1.500000000000002220 ) ) ;
#48862=ORIENTED_EDGE ( 'NONE', *, *, #40204, .T. ) ;
#48867=CARTESIAN_POINT ( 'NONE',  ( 7.950249384483326409, 19.69624408967213469, -1.500000000000002220 ) ) ;
#48869=CARTESIAN_POINT ( 'NONE',  ( -30.59326697242301663, -24.88273649812090227, 8.549170486301877148 ) ) ;
#48870=DIRECTION ( 'NONE',  ( 3.773278334444166432E-23, -1.000000000000000000, 0.000000000000000000 ) ) ;
#48873=CARTESIAN_POINT ( 'NONE',  ( -10.03281922573575002, -16.61734169602722488, -1.500000000000002220 ) ) ;
#48874=CARTESIAN_POINT ( 'NONE',  ( -117.5520235238924158, -24.66019654487200441, 8.947790411086112172 ) ) ;
#48876=CARTESIAN_POINT ( 'NONE',  ( -8.384790838521158918, 17.58144419890746235, 11.49999999999999645 ) ) ;
#48880=EDGE_LOOP ( 'NONE', ( #34452, #77383, #16715, #6894 ) ) ;
#48882=CARTESIAN_POINT ( 'NONE',  ( -75.62287095715011276, -23.85196035786901803, -0.8779234886475031363 ) ) ;
#48884=CARTESIAN_POINT ( 'NONE',  ( -81.73829046040381741, -25.03155895851643464, 6.803918155767815001 ) ) ;
#48885=CARTESIAN_POINT ( 'NONE',  ( 6.681059570357060551, -18.48443787736713873, 11.49999999999998934 ) ) ;
#48886=ORIENTED_EDGE ( 'NONE', *, *, #31089, .F. ) ;
#48887=EDGE_CURVE ( 'NONE', #60374, #79287, #22721, .T. ) ;
#48890=CARTESIAN_POINT ( 'NONE',  ( 19.40787663092975279, -12.54570180764831377, -1.500000000000002220 ) ) ;
#48891=ADVANCED_FACE ( 'NONE', ( #92751 ), #23236, .T. ) ;
#48894=LINE ( 'NONE', #26038, #48331 ) ;
#48896=CARTESIAN_POINT ( 'NONE',  ( -109.4136617073600917, -25.16309701932601328, 3.145511876789759853 ) ) ;
#48897=CARTESIAN_POINT ( 'NONE',  ( -63.52287095715006160, -29.50250786944525672, 11.44777988621623876 ) ) ;
#48900=LINE ( 'NONE', #10323, #89438 ) ;
#48902=CARTESIAN_POINT ( 'NONE',  ( -18.69216024341242743, -6.879743215651725308, -1.500000000000002220 ) ) ;
#48904=DIRECTION ( 'NONE',  ( 1.000000000000000000, 3.773278334444167608E-23, 8.201307833595939069E-29 ) ) ;
#48905=CARTESIAN_POINT ( 'NONE',  ( -10.37884456512175291, 16.95428827495986823, -1.500000000000002220 ) ) ;
#48907=DIRECTION ( 'NONE',  ( -3.773278334453079030E-23, 0.9999999999976377785, 2.173523156925979128E-06 ) ) ;
#48910=CARTESIAN_POINT ( 'NONE',  ( -125.5228709571500900, -24.62226745350437795, 0.9660975649728180681 ) ) ;
#48912=CARTESIAN_POINT ( 'NONE',  ( -8.830788454959730416, 18.81286502489961876, 11.49999999999999645 ) ) ;
#48915=CARTESIAN_POINT ( 'NONE',  ( 21.04450177026006230, 8.645109164175620364, 11.49999999999999645 ) ) ;
#48916=ORIENTED_EDGE ( 'NONE', *, *, #89645, .F. ) ;
#48917=DIRECTION ( 'NONE',  ( 3.773278334444167608E-23, -1.000000000000000000, 0.000000000000000000 ) ) ;
#48920=CARTESIAN_POINT ( 'NONE',  ( -6.636546740042271963, -19.09123619949631134, 11.49999999999998934 ) ) ;
#48923=B_SPLINE_CURVE_WITH_KNOTS ( 'NONE', 3,
 ( #49416, #72747, #21801, #27063 ),
 .UNSPECIFIED., .F., .F.,
 ( 4, 4 ),
 ( 0.000000000000000000, 9.999999999998897304E-05 ),
 .UNSPECIFIED. ) ;
#48925=CARTESIAN_POINT ( 'NONE',  ( -51.62287095715005592, -23.48786465467241413, 11.44779295918254824 ) ) ;
#48926=ORIENTED_EDGE ( 'NONE', *, *, #34997, .T. ) ;
#48928=CARTESIAN_POINT ( 'NONE',  ( -104.5895376238167245, -23.47596703998600631, 11.44779298504227683 ) ) ;
#48929=CARTESIAN_POINT ( 'NONE',  ( -13.81204400269958654, 14.50282280199826701, -1.500000000000002220 ) ) ;
#48930=CARTESIAN_POINT ( 'NONE',  ( 17.15856466979341377, 12.00972951212132855, 11.49999999999999645 ) ) ;
#48931=CARTESIAN_POINT ( 'NONE',  ( -54.62287095715005592, -24.66019654487199020, 8.947790411086135265 ) ) ;
#48932=CARTESIAN_POINT ( 'NONE',  ( -124.6228709571500701, -23.47596703998600631, 11.44779298504227860 ) ) ;
#48933=CARTESIAN_POINT ( 'NONE',  ( 21.84380375219137349, -3.031640915038902762, -1.500000000000002220 ) ) ;
#48935=EDGE_CURVE ( 'NONE', #9106, #18610, #62328, .T. ) ;
#48938=CARTESIAN_POINT ( 'NONE',  ( -60.52287095715006870, -23.84047902841601996, -0.8780736468305723186 ) ) ;
#48940=CARTESIAN_POINT ( 'NONE',  ( -72.58794503245407270, -24.34968618360933590, 0.1864209137778795600 ) ) ;
#48941=ORIENTED_EDGE ( 'NONE', *, *, #98674, .F. ) ;
#48943=ORIENTED_EDGE ( 'NONE', *, *, #21230, .T. ) ;
#48946=LINE ( 'NONE', #86493, #98850 ) ;
#48947=CARTESIAN_POINT ( 'NONE',  ( -58.62287095715006302, -24.34917612406837861, 0.1852690917426618733 ) ) ;
#48948=CARTESIAN_POINT ( 'NONE',  ( 17.96566822227200433, 9.963707542159163211, -1.500000000000002220 ) ) ;
#48949=ORIENTED_EDGE ( 'NONE', *, *, #95999, .T. ) ;
#48952=CARTESIAN_POINT ( 'NONE',  ( -83.52287095715009002, -23.73907113216989373, -1.053371485793249684 ) ) ;
#48953=CARTESIAN_POINT ( 'NONE',  ( -21.40455707349245529, -6.346402434563959361, -1.500000000000002220 ) ) ;
#48954=CARTESIAN_POINT ( 'NONE',  ( -71.25156906290497716, -25.22179730619566840, 6.511357954259892722 ) ) ;
#48957=CARTESIAN_POINT ( 'NONE',  ( -32.08503310962682065, -24.86181185134534388, 1.747789972853592833 ) ) ;
#48959=CARTESIAN_POINT ( 'NONE',  ( -13.77211689728001964, -15.67653869864640903, 11.49999999999998934 ) ) ;
#48961=ORIENTED_EDGE ( 'NONE', *, *, #37976, .F. ) ;
#48963=ORIENTED_EDGE ( 'NONE', *, *, #95900, .T. ) ;
#48965=ORIENTED_EDGE ( 'NONE', *, *, #27804, .T. ) ;
#48966=CARTESIAN_POINT ( 'NONE',  ( -62.62287095715004881, -29.50250243563736774, 8.947779886222145151 ) ) ;
#48967=CARTESIAN_POINT ( 'NONE',  ( -13.78326148797977169, 15.88460234914768421, -1.500000000000002220 ) ) ;
#48970=CARTESIAN_POINT ( 'NONE',  ( -53.52287095715006160, -24.50321055353805377, 9.387540953477522265 ) ) ;
#48971=CARTESIAN_POINT ( 'NONE',  ( -120.6245363983109655, -24.73531770709095312, 8.716586749053508498 ) ) ;
#48973=CARTESIAN_POINT ( 'NONE',  ( -100.9913061220214843, -25.03152431204875583, 7.480517603216952693 ) ) ;
#48974=CARTESIAN_POINT ( 'NONE',  ( -49.55620429048340014, -24.64898659630528499, 1.056161002820822592 ) ) ;
#48975=CARTESIAN_POINT ( 'NONE',  ( 12.10466045530642631, 18.00204671274030233, -1.500000000000002220 ) ) ;
#48977=CARTESIAN_POINT ( 'NONE',  ( -13.27262489239681997, 17.90159134968837051, 11.49999999999999645 ) ) ;
#48979=CARTESIAN_POINT ( 'NONE',  ( -51.52764846858840997, -25.31441937397667274, 6.187572642957288593 ) ) ;
#48980=CARTESIAN_POINT ( 'NONE',  ( -87.52287095715006160, -23.48783264083352762, -1.443836473376473695 ) ) ;
#48982=B_SPLINE_CURVE_WITH_KNOTS ( 'NONE', 3,
 ( #97160, #90047, #20517, #29137 ),
 .UNSPECIFIED., .F., .F.,
 ( 4, 4 ),
 ( 0.5091335765045065243, 0.5101343235452722169 ),
 .UNSPECIFIED. ) ;
#48985=CARTESIAN_POINT ( 'NONE',  ( -118.6228709571500701, -24.50321055353805377, 9.387540953477516936 ) ) ;
#48986=ORIENTED_EDGE ( 'NONE', *, *, #34804, .T. ) ;
#48987=AXIS2_PLACEMENT_3D ( 'NONE', #39614, #70567, #48243 ) ;
#48991=CARTESIAN_POINT ( 'NONE',  ( -57.62287095715004881, -23.47596703998600276, 11.44779298504227683 ) ) ;
#48992=CARTESIAN_POINT ( 'NONE',  ( 5.670567493371958534, -19.34269084982597775, 11.49999999999998934 ) ) ;
#48993=CARTESIAN_POINT ( 'NONE',  ( -66.52287095715006160, -24.64965694238407323, 8.947790433994200043 ) ) ;
#48995=CARTESIAN_POINT ( 'NONE',  ( -130.5728709571501156, -25.24108479417091289, 2.995995577098621077 ) ) ;
#48996=CARTESIAN_POINT ( 'NONE',  ( 15.70178742502441693, -15.98865493379879332, -1.500000000000002220 ) ) ;
#48998=VERTEX_POINT ( 'NONE', #66721 ) ;
#49000=CARTESIAN_POINT ( 'NONE',  ( -112.5952105876609153, -23.48786465467241769, 11.44779295918253936 ) ) ;
#49001=CARTESIAN_POINT ( 'NONE',  ( -101.5193634269438405, -23.73791477778911840, 11.05961554403170588 ) ) ;
#49003=CARTESIAN_POINT ( 'NONE',  ( -129.5228709571500758, -23.47596703998600631, 11.44779298504227683 ) ) ;
#49004=CARTESIAN_POINT ( 'NONE',  ( -97.24578422077173911, -24.82959736273287277, 8.370978854367631783 ) ) ;
#49005=CARTESIAN_POINT ( 'NONE',  ( -12.82114019720147802, -14.77593736753402709, 11.49999999999998934 ) ) ;
#49006=B_SPLINE_SURFACE_WITH_KNOTS ( 'NONE', 3, 1, ( 
 ( #43476, #74413 ),
 ( #45967, #63197 ),
 ( #30730, #275 ),
 ( #24107, #55080 ),
 ( #1290, #15492 ),
 ( #86013, #93613 ),
 ( #94120, #22594 ),
 ( #84513, #16489 ),
 ( #100210, #54570 ),
 ( #46456, #32220 ),
 ( #85508, #77386 ),
 ( #47461, #92616 ),
 ( #69293, #84012 ),
 ( #78388, #53588 ),
 ( #24604, #14499 ) ),
 .UNSPECIFIED., .F., .F., .F.,
 ( 4, 1, 1, 1, 1, 1, 1, 1, 1, 1, 1, 1, 4 ),
 ( 2, 2 ),
 ( 0.000000000000000000, 0.07489820792759518953, 0.1485962943439394779, 0.2244712347857275581, 0.3023227423595722940, 0.3819186179896829625, 0.4611486955215912120, 0.5424171227241534332, 0.6267160830665706728, 0.7145968311855385169, 0.8049029203553225154, 0.9001272540718607829, 1.000000000000000000 ),
 ( 0.000000000000000000, 1.000000000000000000 ),
 .UNSPECIFIED. ) ;
#49007=CARTESIAN_POINT ( 'NONE',  ( -46.59349553319857762, -24.15543982623906416, -0.2315651400026683127 ) ) ;
#49008=ORIENTED_EDGE ( 'NONE', *, *, #50805, .T. ) ;
#49009=CARTESIAN_POINT ( 'NONE',  ( -21.26083644630951142, -3.357327265692296780, 11.49999999999998934 ) ) ;
#49011=CARTESIAN_POINT ( 'NONE',  ( -114.5228709571500474, -24.50216790748205042, 0.6166512839542590552 ) ) ;
#49012=DIRECTION ( 'NONE',  ( 3.773278334444166432E-23, -1.000000000000000000, 0.000000000000000000 ) ) ;
#49013=PLANE ( 'NONE',  #53693 ) ;
#49014=CARTESIAN_POINT ( 'NONE',  ( 7.457602374657920308, -21.66695214233757838, -1.500000000000002220 ) ) ;
#49017=EDGE_CURVE ( 'NONE', #33587, #15382, #48281, .T. ) ;
#49020=CARTESIAN_POINT ( 'NONE',  ( -53.59318146942742089, -24.15543982623906771, -0.2315651400026670359 ) ) ;
#49021=CARTESIAN_POINT ( 'NONE',  ( 7.746586651691365510, 18.53313339873204058, 11.49999999999999645 ) ) ;
#49022=CARTESIAN_POINT ( 'NONE',  ( -109.8914236385200525, -25.28814080510020901, 2.885852232195856182 ) ) ;
#49023=CARTESIAN_POINT ( 'NONE',  ( -90.52287095715006160, -23.48786465467241769, 11.44779295918254292 ) ) ;
#49025=FACE_OUTER_BOUND ( 'NONE', #47848, .T. ) ;
#49026=CARTESIAN_POINT ( 'NONE',  ( -126.5562042904833930, -23.47596703998600631, 11.44779298504227683 ) ) ;
#49027=CARTESIAN_POINT ( 'NONE',  ( -100.6228709571500701, -23.47596703998600631, 11.44779298504227860 ) ) ;
#49028=CARTESIAN_POINT ( 'NONE',  ( 18.78741845327603599, -6.401996767227196905, 11.49999999999998934 ) ) ;
#49030=CARTESIAN_POINT ( 'NONE',  ( -94.52287095715006160, -23.95044443724991723, 10.65354141964649948 ) ) ;
#49031=CARTESIAN_POINT ( 'NONE',  ( -11.90832679833862073, -15.64659449181510986, -1.500000000000002220 ) ) ;
#49032=CARTESIAN_POINT ( 'NONE',  ( -85.52287095715004739, -24.99132157543166954, 2.256160258750667502 ) ) ;
#49038=PLANE ( 'NONE',  #40283 ) ;
#49040=CARTESIAN_POINT ( 'NONE',  ( 9.220172233967117492, 18.46515239161685784, 11.49999999999999645 ) ) ;
#49043=CARTESIAN_POINT ( 'NONE',  ( -17.80605238980536953, 13.89162706601689479, 11.49999999999999645 ) ) ;
#49044=VERTEX_POINT ( 'NONE', #28135 ) ;
#49045=CARTESIAN_POINT ( 'NONE',  ( -69.35973275182155362, -25.12218989444304995, 6.387116372111183438 ) ) ;
#49047=CARTESIAN_POINT ( 'NONE',  ( -97.58871357123791768, -24.34968618360934300, 0.1864209137778856384 ) ) ;
#49048=CARTESIAN_POINT ( 'NONE',  ( -39.62287095715005592, -24.64898659630366851, 1.056161002820819261 ) ) ;
#49049=CARTESIAN_POINT ( 'NONE',  ( -127.5228709571500616, -23.47596703998600631, 11.44779298504227683 ) ) ;
#49053=CARTESIAN_POINT ( 'NONE',  ( 1.767912858038628965, -23.04938964843747584, 11.49999999999999645 ) ) ;
#49054=CARTESIAN_POINT ( 'NONE',  ( -10.82450569625279613, 20.10975305113172951, 11.49999999999998934 ) ) ;
#49056=CARTESIAN_POINT ( 'NONE',  ( -96.54755524882318696, -24.51314013834316086, 0.6176544820404197278 ) ) ;
#49057=CARTESIAN_POINT ( 'NONE',  ( -63.55959558400564902, -23.73791477778911840, 11.05961554403170766 ) ) ;
#49059=CARTESIAN_POINT ( 'NONE',  ( 16.80569330386292748, 14.95695114220347932, 11.49999999999999645 ) ) ;
#49061=CARTESIAN_POINT ( 'NONE',  ( -43.55309799638700952, -23.96119346886880308, -0.6495511937831988103 ) ) ;
#49062=CARTESIAN_POINT ( 'NONE',  ( -3.625624329714521643, -21.66436044012089468, -1.500000000000002220 ) ) ;
#49063=CARTESIAN_POINT ( 'NONE',  ( -54.62287095715006302, -24.51283580621364777, 0.6167428607019743714 ) ) ;
#49064=CARTESIAN_POINT ( 'NONE',  ( -44.62370648846312093, -24.66019654487199375, 8.947790411086115725 ) ) ;
#49065=CARTESIAN_POINT ( 'NONE',  ( -83.62287095715005592, -29.50247984919015209, -1.443849546365053582 ) ) ;
#49067=FACE_OUTER_BOUND ( 'NONE', #30412, .T. ) ;
#49069=ORIENTED_EDGE ( 'NONE', *, *, #9825, .T. ) ;
#49071=CARTESIAN_POINT ( 'NONE',  ( 15.48611046165106941, -13.43736321338083783, -1.500000000000002220 ) ) ;
#49073=ORIENTED_EDGE ( 'NONE', *, *, #76159, .F. ) ;
#49075=ORIENTED_EDGE ( 'NONE', *, *, #90840, .F. ) ;
#49076=B_SPLINE_CURVE_WITH_KNOTS ( 'NONE', 3,
 ( #13083, #20200, #68390, #6488 ),
 .UNSPECIFIED., .F., .F.,
 ( 4, 4 ),
 ( 0.000000000000000000, 9.999999999998897304E-05 ),
 .UNSPECIFIED. ) ;
#49079=CARTESIAN_POINT ( 'NONE',  ( 10.19088217375349892, 20.72639945755932800, 11.49999999999998934 ) ) ;
#49080=CARTESIAN_POINT ( 'NONE',  ( -41.52287095715006870, -23.48786465467240347, 11.44779295918255180 ) ) ;
#49081=CARTESIAN_POINT ( 'NONE',  ( -17.59887021274124663, -10.25344800880639262, -1.500000000000002220 ) ) ;
#49082=ORIENTED_EDGE ( 'NONE', *, *, #88194, .T. ) ;
#49083=FACE_OUTER_BOUND ( 'NONE', #3753, .T. ) ;
#49085=FACE_OUTER_BOUND ( 'NONE', #16873, .T. ) ;
#49087=ORIENTED_EDGE ( 'NONE', *, *, #69523, .T. ) ;
#49088=PLANE ( 'NONE',  #66312 ) ;
#49089=CARTESIAN_POINT ( 'NONE',  ( -49.10457154551148307, -25.26385639663606497, 3.999772272082692037 ) ) ;
#49090=ORIENTED_EDGE ( 'NONE', *, *, #74985, .T. ) ;
#49091=CARTESIAN_POINT ( 'NONE',  ( -20.31193019649481357, 4.361987795224258946, 11.49999999999998934 ) ) ;
#49096=B_SPLINE_CURVE_WITH_KNOTS ( 'NONE', 3,
 ( #21707, #6505, #14102, #7001 ),
 .UNSPECIFIED., .F., .F.,
 ( 4, 4 ),
 ( 0.000000000000000000, 9.999999999998897304E-05 ),
 .UNSPECIFIED. ) ;
#49097=EDGE_CURVE ( 'NONE', #4416, #61038, #28861, .T. ) ;
#49098=B_SPLINE_SURFACE_WITH_KNOTS ( 'NONE', 3, 3, ( 
 ( #76811, #6816, #23020, #32150 ),
 ( #15423, #84938, #8319, #23522 ),
 ( #61125, #46382, #47390, #61629 ),
 ( #53518, #92549, #77316, #30151 ),
 ( #54499, #7817, #31152, #92054 ),
 ( #70223, #14921, #93043, #45894 ),
 ( #62121, #15921, #703, #7310 ) ),
 .UNSPECIFIED., .F., .F., .F.,
 ( 4, 3, 4 ),
 ( 4, 4 ),
 ( 0.7945040050992242531, 0.8970133687736498995, 0.9995227324480754350 ),
 ( 0.08951674469141676638, 0.09057079611598997659 ),
 .UNSPECIFIED. ) ;
#49101=ORIENTED_EDGE ( 'NONE', *, *, #89045, .T. ) ;
#49102=ORIENTED_EDGE ( 'NONE', *, *, #45364, .F. ) ;
#49104=CARTESIAN_POINT ( 'NONE',  ( -58.62287095715004881, -23.47593901973091235, -1.443836447539007972 ) ) ;
#49105=CARTESIAN_POINT ( 'NONE',  ( -28.16513019978995302, -24.66613713371811656, 1.682082916390950533 ) ) ;
#49106=CARTESIAN_POINT ( 'NONE',  ( -21.12782282263547984, 6.412464199276892707, 11.49999999999999645 ) ) ;
#49107=ORIENTED_EDGE ( 'NONE', *, *, #25034, .T. ) ;
#49108=CARTESIAN_POINT ( 'NONE',  ( -103.6250747051918353, -24.51314013834315375, 0.6176544820404142877 ) ) ;
#49110=CARTESIAN_POINT ( 'NONE',  ( -22.20892344277460850, -4.061126821146308963, -1.500000000000002220 ) ) ;
#49112=EDGE_CURVE ( 'NONE', #62582, #16286, #96634, .T. ) ;
#49113=EDGE_CURVE ( 'NONE', #86042, #11910, #9443, .T. ) ;
#49114=CARTESIAN_POINT ( 'NONE',  ( -90.52287095715006160, -23.47593901973090524, -1.443836447538996426 ) ) ;
#49115=ORIENTED_EDGE ( 'NONE', *, *, #59093, .T. ) ;
#49118=EDGE_CURVE ( 'NONE', #5913, #76909, #43431, .T. ) ;
#49119=DIRECTION ( 'NONE',  ( -3.773278334444167608E-23, 1.000000000000000000, 0.000000000000000000 ) ) ;
#49122=CARTESIAN_POINT ( 'NONE',  ( 3.105769797727405024, 20.95935918496786599, 11.49999999999998934 ) ) ;
#49123=CARTESIAN_POINT ( 'NONE',  ( -128.6228709571500417, -29.50248528299804818, 1.056150453629047137 ) ) ;
#49126=CARTESIAN_POINT ( 'NONE',  ( -105.6228709571500275, -25.00182538069145721, 7.747789668545099317 ) ) ;
#49127=CARTESIAN_POINT ( 'NONE',  ( 21.60277357391871433, -5.133695162202882578, -1.500000000000002220 ) ) ;
#49128=FACE_OUTER_BOUND ( 'NONE', #24420, .T. ) ;
#49130=VERTEX_POINT ( 'NONE', #6282 ) ;
#49132=CARTESIAN_POINT ( 'NONE',  ( -50.58953762381672448, -23.47596703998600276, 11.44779298504227505 ) ) ;
#49133=CARTESIAN_POINT ( 'NONE',  ( -4.539579955115475407, -18.87035741768621122, 11.49999999999999645 ) ) ;
#49134=DIRECTION ( 'NONE',  ( 3.773278334444166432E-23, -1.000000000000000000, 0.000000000000000000 ) ) ;
#49135=CARTESIAN_POINT ( 'NONE',  ( -31.52287095715006160, -24.64898659630367206, 1.056161002820817485 ) ) ;
#49138=CARTESIAN_POINT ( 'NONE',  ( 18.23270504744370868, -6.907985942191454676, -1.500000000000002220 ) ) ;
#49140=CARTESIAN_POINT ( 'NONE',  ( 6.977786103627443559, 20.27319509581574408, 11.49999999999998934 ) ) ;
#49142=CARTESIAN_POINT ( 'NONE',  ( -60.62578132507420037, -24.92592662360294042, 8.075495902990192931 ) ) ;
#49144=CARTESIAN_POINT ( 'NONE',  ( -74.62287095715005592, -29.50248528299804818, 1.056150453629036701 ) ) ;
#49145=CARTESIAN_POINT ( 'NONE',  ( -4.508144621425604903, 22.28865971958312997, -1.500000000000002220 ) ) ;
#49147=AXIS2_PLACEMENT_3D ( 'NONE', #95666, #18532, #88556 ) ;
#49151=CARTESIAN_POINT ( 'NONE',  ( -18.79874323561663729, 6.599581278811135654, 11.49999999999999645 ) ) ;
#49152=CARTESIAN_POINT ( 'NONE',  ( -101.6228709571501128, -24.35013146730204525, 9.818937971375103047 ) ) ;
#49154=CARTESIAN_POINT ( 'NONE',  ( -39.64842002074407645, -23.96169478059713143, 10.65365249895718769 ) ) ;
#49157=CARTESIAN_POINT ( 'NONE',  ( -120.6228709571500701, -25.00158670708909625, 2.256160236439166411 ) ) ;
#49159=CARTESIAN_POINT ( 'NONE',  ( -7.614213781628100364, -20.28429660096114517, -1.500000000000002220 ) ) ;
#49160=DIRECTION ( 'NONE',  ( -1.000000000000000000, -3.773278334444167608E-23, -8.201307833595939069E-29 ) ) ;
#49161=CARTESIAN_POINT ( 'NONE',  ( 14.32981562401322506, -13.22600733894156200, -1.500000000000002220 ) ) ;
#49162=CARTESIAN_POINT ( 'NONE',  ( -60.62287095715004881, -24.99132157543084531, 2.256160258750667502 ) ) ;
#49163=EDGE_CURVE ( 'NONE', #40340, #89470, #82053, .T. ) ;
#49164=ORIENTED_EDGE ( 'NONE', *, *, #50242, .F. ) ;
#49165=CARTESIAN_POINT ( 'NONE',  ( -69.62287095715005592, -24.64965695001468404, 8.947790433994184056 ) ) ;
#49166=CARTESIAN_POINT ( 'NONE',  ( -14.48729221511043441, 14.40292172154154926, 11.49999999999999645 ) ) ;
#49167=DIRECTION ( 'NONE',  ( -9.524068072025174096E-40, -2.173523156925980399E-06, 0.9999999999976378895 ) ) ;
#49170=ORIENTED_EDGE ( 'NONE', *, *, #24017, .T. ) ;
#49171=CARTESIAN_POINT ( 'NONE',  ( -74.62287095715005592, -23.48783264082478794, -1.443836473390067265 ) ) ;
#49173=CARTESIAN_POINT ( 'NONE',  ( -113.9228709571500957, -23.47593901973090880, -1.443836447538996870 ) ) ;
#49174=FACE_OUTER_BOUND ( 'NONE', #24704, .T. ) ;
#49175=B_SPLINE_CURVE_WITH_KNOTS ( 'NONE', 3,
 ( #45793, #84340, #14824, #6223 ),
 .UNSPECIFIED., .F., .F.,
 ( 4, 4 ),
 ( 0.000000000000000000, 9.999999999998897304E-05 ),
 .UNSPECIFIED. ) ;
#49180=CARTESIAN_POINT ( 'NONE',  ( -82.52287095715006160, -23.47593901973090169, -1.443836447538996648 ) ) ;
#49181=CARTESIAN_POINT ( 'NONE',  ( 22.95104020007722667, -0.4190376320207603866, 11.49999999999999645 ) ) ;
#49182=CARTESIAN_POINT ( 'NONE',  ( 10.97283692364161922, -19.94330716608196852, -1.500000000000002220 ) ) ;
#49183=CARTESIAN_POINT ( 'NONE',  ( -110.5864147487693288, -24.92592662359561828, 8.075495903018000021 ) ) ;
#49186=CARTESIAN_POINT ( 'NONE',  ( -90.63674641968886192, -24.15503026093915651, -0.2815557561904460382 ) ) ;
#49188=CARTESIAN_POINT ( 'NONE',  ( -89.52287095715007581, -23.73907113217668297, -1.053371485781303907 ) ) ;
#49189=CARTESIAN_POINT ( 'NONE',  ( -13.92312151449838531, -16.86485062357919773, 11.49999999999998934 ) ) ;
#49190=DIRECTION ( 'NONE',  ( -3.773278334453080206E-23, 0.9999999999976377785, 2.173523156925979975E-06 ) ) ;
#49191=CARTESIAN_POINT ( 'NONE',  ( -115.6228709571500417, -23.48783264082478794, -1.443836473390058384 ) ) ;
#49193=CARTESIAN_POINT ( 'NONE',  ( -58.50879486179008637, -23.96119346886881019, -0.6495511937832116889 ) ) ;
#49194=VERTEX_POINT ( 'NONE', #53475 ) ;
#49195=CARTESIAN_POINT ( 'NONE',  ( -18.43012528856881715, -8.789534013050598560, 11.49999999999998934 ) ) ;
#49196=ORIENTED_EDGE ( 'NONE', *, *, #33752, .F. ) ;
#49198=CARTESIAN_POINT ( 'NONE',  ( -6.685540227124203483, -22.02754839873749404, 11.49999999999998934 ) ) ;
#49201=CARTESIAN_POINT ( 'NONE',  ( -109.8650237084402619, -25.29042187987247914, 5.784623108531866897 ) ) ;
#49202=CARTESIAN_POINT ( 'NONE',  ( -76.62287095715007013, -24.64965695001468404, 8.947790433994182280 ) ) ;
#49203=VECTOR ( 'NONE', #58972, 1000.000000000000114 ) ;
#49204=CARTESIAN_POINT ( 'NONE',  ( -98.62287095715009855, -24.51387760970724372, 9.387446482453414731 ) ) ;
#49205=CARTESIAN_POINT ( 'NONE',  ( -96.62287095715005592, -24.50216790748097750, 0.6166512839513716981 ) ) ;
#49206=CARTESIAN_POINT ( 'NONE',  ( 2.936642053869352953, -21.15864249054145674, 11.49999999999999645 ) ) ;
#49209=CARTESIAN_POINT ( 'NONE',  ( -19.85906585229243504, 9.992431322412627992, -1.500000000000002220 ) ) ;
#49210=CARTESIAN_POINT ( 'NONE',  ( 7.914317726235799100, 19.11507755054979896, 11.49999999999998934 ) ) ;
#49214=CARTESIAN_POINT ( 'NONE',  ( -41.62287095715006302, -29.50247984919015209, -1.443849546365060466 ) ) ;
#49217=LINE ( 'NONE', #86752, #94777 ) ;
#49222=CARTESIAN_POINT ( 'NONE',  ( 8.587038044527741221, -19.06309208085484386, -1.500000000000002220 ) ) ;
#49223=CARTESIAN_POINT ( 'NONE',  ( -11.18773875818744656, -18.78983145652188469, 11.49999999999999645 ) ) ;
#49224=EDGE_CURVE ( 'NONE', #70309, #46658, #2273, .T. ) ;
#49225=CARTESIAN_POINT ( 'NONE',  ( -68.62287095715005592, -29.50248528299804818, 1.056150453629036701 ) ) ;
#49227=CARTESIAN_POINT ( 'NONE',  ( 22.48772827135616126, 0.8316936486096353498, -1.500000000000002220 ) ) ;
#49229=CARTESIAN_POINT ( 'NONE',  ( -3.950822543831816080, -20.53616823614468956, -1.500000000000002220 ) ) ;
#49230=CARTESIAN_POINT ( 'NONE',  ( -38.63478458652770087, -24.34968618360933235, 0.1864209137778849723 ) ) ;
#49233=ORIENTED_EDGE ( 'NONE', *, *, #63206, .T. ) ;
#49236=CARTESIAN_POINT ( 'NONE',  ( -52.54159836110628135, -24.34968618360933945, 0.1864209137778880532 ) ) ;
#49237=ORIENTED_EDGE ( 'NONE', *, *, #27357, .F. ) ;
#49238=CARTESIAN_POINT ( 'NONE',  ( -21.38522110535750542, 1.317000383210971792, -1.500000000000002220 ) ) ;
#49240=CARTESIAN_POINT ( 'NONE',  ( 21.86734719908870872, 4.625976558377421277, 11.49999999999999645 ) ) ;
#49241=ORIENTED_EDGE ( 'NONE', *, *, #89712, .T. ) ;
#49243=CARTESIAN_POINT ( 'NONE',  ( 2.841100885065937387, 20.89556961663114265, -1.500000000000002220 ) ) ;
#49244=CARTESIAN_POINT ( 'NONE',  ( -30.40788173565302088, -25.13746717394300845, 7.291421475381016926 ) ) ;
#49248=CARTESIAN_POINT ( 'NONE',  ( -101.5471480383779408, -24.65952944569305316, 1.056160979905706121 ) ) ;
#49249=CARTESIAN_POINT ( 'NONE',  ( 21.54648482299927181, -4.703075207800759827, -1.500000000000002220 ) ) ;
#49251=CARTESIAN_POINT ( 'NONE',  ( -65.55949235626067662, -23.85049219812685806, 10.88485053497527311 ) ) ;
#49253=CARTESIAN_POINT ( 'NONE',  ( -111.6228709571500417, -24.66019654487199730, 8.947790411086124607 ) ) ;
#49254=CARTESIAN_POINT ( 'NONE',  ( -60.52842363010253735, -25.00158670708910336, 2.256160236439220590 ) ) ;
#49255=CARTESIAN_POINT ( 'NONE',  ( -62.57945178327253899, -24.66019654487199730, 8.947790411086124607 ) ) ;
#49256=B_SPLINE_CURVE_WITH_KNOTS ( 'NONE', 3,
 ( #83361, #68651, #5744, #13847 ),
 .UNSPECIFIED., .F., .F.,
 ( 4, 4 ),
 ( 0.000000000000000000, 9.999999999998898659E-05 ),
 .UNSPECIFIED. ) ;
#49258=CARTESIAN_POINT ( 'NONE',  ( -25.53098197642538736, -24.91566218739149363, 4.942811707542018596 ) ) ;
#49259=CARTESIAN_POINT ( 'NONE',  ( -117.5228709571500758, -24.34917612406837151, 0.1852690917426621509 ) ) ;
#49260=CARTESIAN_POINT ( 'NONE',  ( -14.61619677566029729, 15.53698580111986693, 11.49999999999998934 ) ) ;
#49261=CARTESIAN_POINT ( 'NONE',  ( -92.22287095715003602, -23.47596703998600631, 11.44779298504227683 ) ) ;
#49263=DIRECTION ( 'NONE',  ( -3.773278334453079618E-23, 0.9999999999976377785, 2.173523156925979975E-06 ) ) ;
#49265=CARTESIAN_POINT ( 'NONE',  ( 6.619388286264371146, -21.57091762011834390, -1.500000000000002220 ) ) ;
#49271=CARTESIAN_POINT ( 'NONE',  ( -0.6023826358649750912, 19.72334862104828090, 11.49999999999999645 ) ) ;
#49272=CARTESIAN_POINT ( 'NONE',  ( -66.62287095715005592, -29.50250786944525672, 11.44777988621623699 ) ) ;
#49278=CARTESIAN_POINT ( 'NONE',  ( -126.6228709571501128, -24.50321055353807509, 9.387540953477524042 ) ) ;
#49280=DIRECTION ( 'NONE',  ( 0.000000000000000000, -0.9999999999976377785, -2.173523156925979128E-06 ) ) ;
#49281=CARTESIAN_POINT ( 'NONE',  ( -74.52287095715007581, -23.47593901973090169, -1.443836447538996870 ) ) ;
#49282=EDGE_CURVE ( 'NONE', #38251, #86491, #14383, .T. ) ;
#49283=CARTESIAN_POINT ( 'NONE',  ( -19.76903914530799966, 0.2396048511829373395, -1.500000000000002220 ) ) ;
#49284=ORIENTED_EDGE ( 'NONE', *, *, #6681, .F. ) ;
#49285=CARTESIAN_POINT ( 'NONE',  ( -6.636546740042271963, -19.09123619949631134, 11.49999999999999645 ) ) ;
#49287=ADVANCED_FACE ( 'NONE', ( #15380 ), #601, .T. ) ;
#49288=ORIENTED_EDGE ( 'NONE', *, *, #35756, .F. ) ;
#49290=CARTESIAN_POINT ( 'NONE',  ( -41.55620429048338593, -23.47596703998600276, 11.44779298504227505 ) ) ;
#49292=CARTESIAN_POINT ( 'NONE',  ( -122.5228709571500616, -23.47596703998600631, 11.44779298504227860 ) ) ;
#49293=CARTESIAN_POINT ( 'NONE',  ( -103.6228709571500417, -23.47596703998600631, 11.44779298504227860 ) ) ;
#49294=CARTESIAN_POINT ( 'NONE',  ( -81.52287095715006160, -24.65952944569304606, 1.056160979905698794 ) ) ;
#49295=CARTESIAN_POINT ( 'NONE',  ( 17.67427751897593069, 9.450557017276361549, -1.500000000000002220 ) ) ;
#49297=EDGE_LOOP ( 'NONE', ( #54544, #61221, #32518, #97745 ) ) ;
#49298=CARTESIAN_POINT ( 'NONE',  ( -51.52287095715006870, -23.96127896941631619, -0.6493128931038041340 ) ) ;
#49299=CARTESIAN_POINT ( 'NONE',  ( -35.62991159852106904, -24.83618233451448987, 1.606449574219547261 ) ) ;
#49302=CARTESIAN_POINT ( 'NONE',  ( -101.7587712593593636, -25.25648092924479826, 3.908092476104340296 ) ) ;
#49305=FACE_OUTER_BOUND ( 'NONE', #43697, .T. ) ;
#49306=ORIENTED_EDGE ( 'NONE', *, *, #30509, .T. ) ;
#49307=CARTESIAN_POINT ( 'NONE',  ( -20.26613141553852060, -1.498020344548873561, -1.500000000000002220 ) ) ;
#49308=VERTEX_POINT ( 'NONE', #70681 ) ;
#49309=CARTESIAN_POINT ( 'NONE',  ( -32.51246533390832383, -23.73766607897670866, -1.055555164236441801 ) ) ;
#49310=VECTOR ( 'NONE', #29062, 1000.000000000000114 ) ;
#49311=CARTESIAN_POINT ( 'NONE',  ( -127.5550739197475139, -24.66019654487200441, 8.947790411086106843 ) ) ;
#49313=FACE_OUTER_BOUND ( 'NONE', #14599, .T. ) ;
#49314=B_SPLINE_CURVE_WITH_KNOTS ( 'NONE', 3,
 ( #16813, #92430, #47778, #31534 ),
 .UNSPECIFIED., .F., .F.,
 ( 4, 4 ),
 ( 0.2799858555236601210, 0.2889922867957759878 ),
 .UNSPECIFIED. ) ;
#49315=CARTESIAN_POINT ( 'NONE',  ( -49.35312698006249832, -25.12215289943983265, 6.504948950085263526 ) ) ;
#49317=DIRECTION ( 'NONE',  ( 1.000000000000000000, 3.773278334444167608E-23, 8.201307833595939069E-29 ) ) ;
#49318=CARTESIAN_POINT ( 'NONE',  ( 10.98566517548414012, -18.08203305749968592, 11.49999999999999645 ) ) ;
#49319=CARTESIAN_POINT ( 'NONE',  ( 19.07224962250127831, -11.27678277851665634, 11.49999999999998934 ) ) ;
#49320=CARTESIAN_POINT ( 'NONE',  ( 13.18781518674367348, -15.76626393773247337, 11.49999999999998934 ) ) ;
#49321=ORIENTED_EDGE ( 'NONE', *, *, #11213, .F. ) ;
#49322=CARTESIAN_POINT ( 'NONE',  ( -91.58953762381672448, -23.47596703998600631, 11.44779298504227683 ) ) ;
#49325=CARTESIAN_POINT ( 'NONE',  ( -58.52287095715006160, -29.50250786944525672, 11.44777988621623876 ) ) ;
#49326=ORIENTED_EDGE ( 'NONE', *, *, #35493, .F. ) ;
#49328=ORIENTED_EDGE ( 'NONE', *, *, #57819, .T. ) ;
#49330=CARTESIAN_POINT ( 'NONE',  ( -112.6228709571501554, -24.34917612406838572, 0.1852690917426693118 ) ) ;
#49332=CARTESIAN_POINT ( 'NONE',  ( -91.62287095715005592, -24.51283580621363711, 0.6167428607019886933 ) ) ;
#49333=CARTESIAN_POINT ( 'NONE',  ( -16.33875328525262560, 12.67428768300982256, -1.500000000000002220 ) ) ;
#49334=CARTESIAN_POINT ( 'NONE',  ( -18.79206335510377102, -10.79472360063173397, 11.49999999999999645 ) ) ;
#49336=EDGE_CURVE ( 'NONE', #97163, #52247, #85904, .T. ) ;
#49339=CARTESIAN_POINT ( 'NONE',  ( 15.70178742502441693, -15.98865493379879332, -1.500000000000002220 ) ) ;
#49343=ORIENTED_EDGE ( 'NONE', *, *, #10265, .F. ) ;
#49345=PLANE ( 'NONE',  #60473 ) ;
#49347=ORIENTED_EDGE ( 'NONE', *, *, #35907, .F. ) ;
#49350=CARTESIAN_POINT ( 'NONE',  ( -46.62845405595144399, -24.51419770103157347, 9.386484678747180510 ) ) ;
#49351=EDGE_LOOP ( 'NONE', ( #82240, #89016, #57195, #22431 ) ) ;
#49353=CARTESIAN_POINT ( 'NONE',  ( 6.361473516681357410, -20.28576754457002451, -1.500000000000002220 ) ) ;
#49355=CARTESIAN_POINT ( 'NONE',  ( -88.63180385516216120, -24.15543982623907837, -0.2315651400026634832 ) ) ;
#49356=CARTESIAN_POINT ( 'NONE',  ( 6.711561834375728175, -20.75310922853297058, -1.500000000000002220 ) ) ;
#49357=CARTESIAN_POINT ( 'NONE',  ( -52.49087273462620118, -24.51419770103158413, 9.386484678747187615 ) ) ;
#49358=B_SPLINE_CURVE_WITH_KNOTS ( 'NONE', 3,
 ( #89748, #12616, #43575, #74514, #5006, #91731 ),
 .UNSPECIFIED., .F., .F.,
 ( 4, 2, 4 ),
 ( 0.000000000000000000, 0.001380901958385383991, 0.002761803916770767982 ),
 .UNSPECIFIED. ) ;
#49359=DIRECTION ( 'NONE',  ( -3.773278334453080206E-23, 0.9999999999976377785, 2.173523156925979975E-06 ) ) ;
#49361=CARTESIAN_POINT ( 'NONE',  ( -15.17958814119055155, -15.74432251006154715, -1.500000000000002220 ) ) ;
#49363=ORIENTED_EDGE ( 'NONE', *, *, #87565, .F. ) ;
#49364=ADVANCED_FACE ( 'NONE', ( #95519 ), #37844, .T. ) ;
#49366=CARTESIAN_POINT ( 'NONE',  ( -85.60742799767531608, -23.48786465467240703, 11.44779295918254647 ) ) ;
#49369=ORIENTED_EDGE ( 'NONE', *, *, #58219, .F. ) ;
#49370=CARTESIAN_POINT ( 'NONE',  ( -58.62287095715004881, -29.50248528299804818, 1.056150453629034924 ) ) ;
#49371=CARTESIAN_POINT ( 'NONE',  ( -82.56324448010200001, -23.48783264082478439, -1.443836473390069486 ) ) ;
#49372=CARTESIAN_POINT ( 'NONE',  ( -7.948041996521916452, 19.69052605537007850, 11.49999999999998934 ) ) ;
#49374=CARTESIAN_POINT ( 'NONE',  ( -30.60515864328932878, -24.57438384523503316, 0.5319095616429412310 ) ) ;
#49376=CARTESIAN_POINT ( 'NONE',  ( -114.5228709571500616, -24.64898659630529565, 1.056161002820831474 ) ) ;
#49377=CARTESIAN_POINT ( 'NONE',  ( -68.64045969480598330, -23.96119346886880663, -0.6495511937832112448 ) ) ;
#49378=CARTESIAN_POINT ( 'NONE',  ( 7.440116899146960172, 17.95454168335740874, -1.500000000000002220 ) ) ;
#49379=CARTESIAN_POINT ( 'NONE',  ( -45.48070769923166523, -24.73486907724918282, 1.287355809206962576 ) ) ;
#49380=ORIENTED_EDGE ( 'NONE', *, *, #58258, .F. ) ;
#49381=CARTESIAN_POINT ( 'NONE',  ( -7.007757480239389380, 18.17491015770016816, 11.49999999999999645 ) ) ;
#49383=B_SPLINE_CURVE_WITH_KNOTS ( 'NONE', 3,
 ( #40059, #63414, #55798, #48178 ),
 .UNSPECIFIED., .F., .F.,
 ( 4, 4 ),
 ( 4.653101527641955381E-09, 0.0004001893594499267054 ),
 .UNSPECIFIED. ) ;
#49384=CARTESIAN_POINT ( 'NONE',  ( -28.67218957988115235, -24.78612079304045679, 7.984269984107190687 ) ) ;
#49387=AXIS2_PLACEMENT_3D ( 'NONE', #74510, #42586, #51687 ) ;
#49389=CARTESIAN_POINT ( 'NONE',  ( -89.50577417353618159, -24.51314013834317862, 0.6176544820404262781 ) ) ;
#49391=EDGE_CURVE ( 'NONE', #10252, #20796, #97514, .T. ) ;
#49392=CARTESIAN_POINT ( 'NONE',  ( -29.62287095715004881, -24.57333416927490433, 1.056161302446588124 ) ) ;
#49393=CARTESIAN_POINT ( 'NONE',  ( 11.96684523812195700, 15.63349346248531546, 11.49999999999998934 ) ) ;
#49394=EDGE_LOOP ( 'NONE', ( #58671, #82999, #26352, #94465 ) ) ;
#49395=PLANE ( 'NONE',  #35925 ) ;
#49396=B_SPLINE_CURVE_WITH_KNOTS ( 'NONE', 3,
 ( #4200, #35154, #10810, #56001 ),
 .UNSPECIFIED., .F., .F.,
 ( 4, 4 ),
 ( 0.000000000000000000, 9.999999999998897304E-05 ),
 .UNSPECIFIED. ) ;
#49397=CARTESIAN_POINT ( 'NONE',  ( -3.594920434497504758, 22.80983129501555950, -1.500000000000002220 ) ) ;
#49399=EDGE_CURVE ( 'NONE', #27352, #95575, #11281, .T. ) ;
#49400=ORIENTED_EDGE ( 'NONE', *, *, #18593, .F. ) ;
#49401=DIRECTION ( 'NONE',  ( 1.000000000000000000, 3.773278334444166432E-23, 8.201307841325785021E-29 ) ) ;
#49403=CARTESIAN_POINT ( 'NONE',  ( -109.4831753910024901, -25.15417620785191133, 3.089146885367800799 ) ) ;
#49404=DIRECTION ( 'NONE',  ( -3.773278334453080206E-23, 0.9999999999976377785, 2.173523156925979975E-06 ) ) ;
#49406=CARTESIAN_POINT ( 'NONE',  ( -69.45824367449309023, -25.31201693057247937, 5.785093212486929204 ) ) ;
#49407=CARTESIAN_POINT ( 'NONE',  ( -73.52287095715007581, -23.47593901973090169, -1.443836447538996870 ) ) ;
#49408=CARTESIAN_POINT ( 'NONE',  ( -6.132916590032589710, 18.96384228413732842, -1.500000000000002220 ) ) ;
#49409=EDGE_CURVE ( 'NONE', #51679, #63420, #65006, .T. ) ;
#49410=B_SPLINE_CURVE_WITH_KNOTS ( 'NONE', 3,
 ( #23146, #42423, #95685, #87571 ),
 .UNSPECIFIED., .F., .F.,
 ( 4, 4 ),
 ( 0.8804146069980227640, 0.8894210382701381867 ),
 .UNSPECIFIED. ) ;
#49411=CARTESIAN_POINT ( 'NONE',  ( -39.62287095715005592, -29.50248528299804818, 1.056150453629031594 ) ) ;
#49412=CARTESIAN_POINT ( 'NONE',  ( 19.48829924427396421, 3.997931079995220127, -1.500000000000002220 ) ) ;
#49415=CARTESIAN_POINT ( 'NONE',  ( -125.5228709571500616, -23.47593901973090524, -1.443836447538996204 ) ) ;
#49416=CARTESIAN_POINT ( 'NONE',  ( -72.62287095715005592, -24.64898659630367916, 1.056161002820824368 ) ) ;
#49419=CARTESIAN_POINT ( 'NONE',  ( 19.16185898538474675, 8.078635803559651052, 11.49999999999999645 ) ) ;
#49422=CARTESIAN_POINT ( 'NONE',  ( -50.50951590840232797, -25.18536261067197302, 3.296990267075738501 ) ) ;
#49423=CARTESIAN_POINT ( 'NONE',  ( 17.70901601935662839, 14.43836031950349152, 11.49999999999999645 ) ) ;
#49425=CARTESIAN_POINT ( 'NONE',  ( -103.5228709571500758, -29.50250786944525672, 11.44777988621623166 ) ) ;
#49427=ORIENTED_EDGE ( 'NONE', *, *, #56796, .F. ) ;
#49428=CARTESIAN_POINT ( 'NONE',  ( 6.697674113365701842, 19.09646837838083400, 11.49999999999998934 ) ) ;
#49432=ORIENTED_EDGE ( 'NONE', *, *, #87194, .F. ) ;
#49433=CARTESIAN_POINT ( 'NONE',  ( -79.61344979208379868, -25.31277616797718366, 5.267994557577900139 ) ) ;
#49435=CARTESIAN_POINT ( 'NONE',  ( -14.92271332039470444, 13.28099397388983327, -1.500000000000002220 ) ) ;
#49436=CARTESIAN_POINT ( 'NONE',  ( -20.39251343623233836, 4.912230638944180328, 11.49999999999999645 ) ) ;
#49437=CARTESIAN_POINT ( 'NONE',  ( -28.59609234217529306, -24.77774177186768156, 8.035888287207853864 ) ) ;
#49438=CARTESIAN_POINT ( 'NONE',  ( -79.58953762381673869, -24.64965694238406968, 8.947790433994654791 ) ) ;
#49439=CARTESIAN_POINT ( 'NONE',  ( 21.39010012190943755, 5.354582491813655309, 11.49999999999998934 ) ) ;
#49441=CARTESIAN_POINT ( 'NONE',  ( -107.5228709571501042, -24.66019654487199730, 8.947790411086115725 ) ) ;
#49442=ORIENTED_EDGE ( 'NONE', *, *, #68826, .F. ) ;
#49443=DIRECTION ( 'NONE',  ( 0.000000000000000000, -2.173523156925980399E-06, 0.9999999999976378895 ) ) ;
#49444=CARTESIAN_POINT ( 'NONE',  ( -118.5228709571500758, -24.64898659630368627, 1.056161002820833028 ) ) ;
#49445=DIRECTION ( 'NONE',  ( -0.000000000000000000, 2.173523156925979552E-06, -0.9999999999976378895 ) ) ;
#49446=ORIENTED_EDGE ( 'NONE', *, *, #60712, .T. ) ;
#49447=DIRECTION ( 'NONE',  ( -1.000000000000000000, -3.773278334444167608E-23, -8.201307833595939069E-29 ) ) ;
#49449=ORIENTED_EDGE ( 'NONE', *, *, #48200, .F. ) ;
#49450=EDGE_CURVE ( 'NONE', #49130, #61311, #50855, .T. ) ;
#49452=DIRECTION ( 'NONE',  ( -3.773278334453079030E-23, 0.9999999999976377785, 2.173523156925979128E-06 ) ) ;
#49453=CARTESIAN_POINT ( 'NONE',  ( -122.5228709571500616, -23.48786465467241769, 11.44779295918253759 ) ) ;
#49454=CARTESIAN_POINT ( 'NONE',  ( 11.66944253441096002, 16.90307425063352298, -1.500000000000002220 ) ) ;
#49460=CARTESIAN_POINT ( 'NONE',  ( -16.35649155429130985, -15.18990082740072367, -1.500000000000002220 ) ) ;
#49461=AXIS2_PLACEMENT_3D ( 'NONE', #18474, #49445, #58060 ) ;
#49464=ORIENTED_EDGE ( 'NONE', *, *, #77694, .F. ) ;
#49465=CARTESIAN_POINT ( 'NONE',  ( -43.58953762381671737, -24.65952944569304606, 1.056160979905696351 ) ) ;
#49467=EDGE_CURVE ( 'NONE', #76836, #48580, #98931, .T. ) ;
#49468=CARTESIAN_POINT ( 'NONE',  ( -2.238888094254589234, -20.74146561784671761, -1.500000000000002220 ) ) ;
#49469=ADVANCED_FACE ( 'NONE', ( #73684 ), #43738, .T. ) ;
#49470=ORIENTED_EDGE ( 'NONE', *, *, #77187, .T. ) ;
#49475=CARTESIAN_POINT ( 'NONE',  ( -8.945158345017247825, -19.07159632999312393, -1.500000000000002220 ) ) ;
#49476=ORIENTED_EDGE ( 'NONE', *, *, #84017, .T. ) ;
#49479=CARTESIAN_POINT ( 'NONE',  ( -120.5884185014208612, -24.83644354573579349, 8.397322867130096569 ) ) ;
#49480=CARTESIAN_POINT ( 'NONE',  ( -86.54785887183577131, -24.35071581493543391, 9.817618358456027039 ) ) ;
#49481=CARTESIAN_POINT ( 'NONE',  ( -36.55620429048339304, -24.65952944569304606, 1.056160979905692132 ) ) ;
#49482=CARTESIAN_POINT ( 'NONE',  ( -21.25272785503416273, -4.502612752106283978, -1.500000000000002220 ) ) ;
#49483=CARTESIAN_POINT ( 'NONE',  ( -63.52287095715006160, -24.51387760970724372, 9.387446482453409402 ) ) ;
#49484=CARTESIAN_POINT ( 'NONE',  ( -8.840690135214121170, 20.45858245768130956, 11.49999999999999645 ) ) ;
#49487=CARTESIAN_POINT ( 'NONE',  ( -51.27521478229555640, -25.24728804126394621, 5.568540310635312629 ) ) ;
#49489=CARTESIAN_POINT ( 'NONE',  ( -71.29929988823592169, -25.25728961307881093, 6.086721405243116223 ) ) ;
#49490=VERTEX_POINT ( 'NONE', #42751 ) ;
#49493=ORIENTED_EDGE ( 'NONE', *, *, #85502, .F. ) ;
#49499=CARTESIAN_POINT ( 'NONE',  ( -42.62287095715004881, -23.48786465467240347, 11.44779295918255180 ) ) ;
#49500=CARTESIAN_POINT ( 'NONE',  ( -4.914914792326205983, -21.87198836336805385, -1.500000000000002220 ) ) ;
#49501=ORIENTED_EDGE ( 'NONE', *, *, #76721, .F. ) ;
#49502=DIRECTION ( 'NONE',  ( -3.773278334453079030E-23, 0.9999999999976377785, 2.173523156925979128E-06 ) ) ;
#49503=CARTESIAN_POINT ( 'NONE',  ( -94.56143569909596636, -23.48786465467241058, 11.44779295918254469 ) ) ;
#49504=CARTESIAN_POINT ( 'NONE',  ( -39.45226965286418164, -25.29606862819456836, 4.310991840858520163 ) ) ;
#49506=CARTESIAN_POINT ( 'NONE',  ( -30.60910590307086565, -24.37907397113049512, 9.703205396196695531 ) ) ;
#49507=EDGE_CURVE ( 'NONE', #81696, #71483, #2094, .T. ) ;
#49508=B_SPLINE_CURVE_WITH_KNOTS ( 'NONE', 3,
 ( #33408, #27303, #56774, #18189, #42045, #58264 ),
 .UNSPECIFIED., .F., .F.,
 ( 4, 2, 4 ),
 ( 6.384118678612889102E-06, 0.001386860460828375635, 0.002767336802978138423 ),
 .UNSPECIFIED. ) ;
#49509=CARTESIAN_POINT ( 'NONE',  ( 13.16580039582533423, -14.52177825760336205, -1.500000000000002220 ) ) ;
#49510=CARTESIAN_POINT ( 'NONE',  ( -87.52287095715006160, -23.47593901973090524, -1.443836447538996648 ) ) ;
#49512=CARTESIAN_POINT ( 'NONE',  ( -15.55086147716002110, 14.89234021980106881, 11.49999999999998934 ) ) ;
#49513=CARTESIAN_POINT ( 'NONE',  ( -75.55620429048337883, -25.00182538069145721, 7.747789668545099317 ) ) ;
#49514=CARTESIAN_POINT ( 'NONE',  ( -71.01839045479064794, -25.12219088163715952, 6.841307120826038535 ) ) ;
#49515=FACE_OUTER_BOUND ( 'NONE', #96867, .T. ) ;
#49517=CARTESIAN_POINT ( 'NONE',  ( 20.74614131242519477, 9.816050768296040729, -1.500000000000002220 ) ) ;
#49522=CARTESIAN_POINT ( 'NONE',  ( -31.58953762381672092, -24.66019654487198665, 8.947790411086138818 ) ) ;
#49523=CARTESIAN_POINT ( 'NONE',  ( -49.55329769530813167, -23.96119346886879953, -0.6495511937832113558 ) ) ;
#49524=CARTESIAN_POINT ( 'NONE',  ( 16.71511084712224360, -11.16500066668146829, 11.49999999999999645 ) ) ;
#49526=CARTESIAN_POINT ( 'NONE',  ( -32.54530050952666898, -24.15620529776627734, 10.23563542870661358 ) ) ;
#49527=AXIS2_PLACEMENT_3D ( 'NONE', #92267, #67955, #90281 ) ;
#49528=CARTESIAN_POINT ( 'NONE',  ( -121.6228709571500417, -24.64965695001469115, 8.947790433994175174 ) ) ;
#49529=CARTESIAN_POINT ( 'NONE',  ( -102.5562042904833788, -24.64898659630528499, 1.056161002820828143 ) ) ;
#49531=CARTESIAN_POINT ( 'NONE',  ( -15.99800673754971037, 11.70972097625665675, 11.49999999999998934 ) ) ;
#49532=AXIS2_PLACEMENT_3D ( 'NONE', #30225, #61699, #44474 ) ;
#49534=CARTESIAN_POINT ( 'NONE',  ( -10.80270875523330965, -16.48872379891551532, -1.500000000000002220 ) ) ;
#49538=CARTESIAN_POINT ( 'NONE',  ( -57.52287095715007581, -23.72773821059536914, 11.05748984161097326 ) ) ;
#49540=CARTESIAN_POINT ( 'NONE',  ( -11.82494684808912844, 16.90534455221803967, 11.49999999999999645 ) ) ;
#49541=EDGE_CURVE ( 'NONE', #61801, #78854, #92815, .T. ) ;
#49543=CARTESIAN_POINT ( 'NONE',  ( -10.49914784070103124, -20.09245350529190688, 11.49999999999999645 ) ) ;
#49545=CARTESIAN_POINT ( 'NONE',  ( -69.45438311041971247, -25.25639499014904743, 6.630172782259688091 ) ) ;
#49546=CARTESIAN_POINT ( 'NONE',  ( -97.50898914409353324, -24.51314013834316086, 0.6176544820404162861 ) ) ;
#49547=CARTESIAN_POINT ( 'NONE',  ( -110.5228709571500332, -24.83602698348160231, 1.605859176311259295 ) ) ;
#49551=EDGE_LOOP ( 'NONE', ( #48458, #69012, #16527, #7677 ) ) ;
#49552=CARTESIAN_POINT ( 'NONE',  ( -79.51137944035450289, -25.26749968020931192, 5.389239678618733542 ) ) ;
#49553=CARTESIAN_POINT ( 'NONE',  ( -19.65108876255925807, -11.61119296138784662, 11.49999999999998934 ) ) ;
#49554=CARTESIAN_POINT ( 'NONE',  ( -74.62362428499353939, -24.65952944569304606, 1.056160979905701680 ) ) ;
#49556=CARTESIAN_POINT ( 'NONE',  ( -82.54711958133198380, -24.35071581493543036, 9.817618358456032368 ) ) ;
#49558=CARTESIAN_POINT ( 'NONE',  ( 5.070899574700155732, -21.93562493352797915, 11.49999999999999645 ) ) ;
#49560=CARTESIAN_POINT ( 'NONE',  ( -111.5228709571500758, -24.66019654487200441, 8.947790411086108620 ) ) ;
#49561=CARTESIAN_POINT ( 'NONE',  ( -6.887433846447126307, -20.85920400149894149, -1.500000000000002220 ) ) ;
#49562=CARTESIAN_POINT ( 'NONE',  ( -127.2834313257731367, -25.38352531986206273, 4.245363004327343148 ) ) ;
#49563=CARTESIAN_POINT ( 'NONE',  ( -111.5524851600246734, -24.34968618360933945, 0.1864209137778883862 ) ) ;
#49564=CARTESIAN_POINT ( 'NONE',  ( -70.25279295878802088, -25.03356033692018912, 7.559852777879553010 ) ) ;
#49566=CARTESIAN_POINT ( 'NONE',  ( -48.63974770086845467, -24.15620529776627734, 10.23563542870660470 ) ) ;
#49569=CARTESIAN_POINT ( 'NONE',  ( -88.52287095715007581, -24.33832256527049509, 0.1851278514138626485 ) ) ;
#49570=CARTESIAN_POINT ( 'NONE',  ( 14.40702264168333890, -14.58922348230443689, 11.49999999999998934 ) ) ;
#49571=ORIENTED_EDGE ( 'NONE', *, *, #84368, .T. ) ;
#49573=VERTEX_POINT ( 'NONE', #86726 ) ;
#49574=EDGE_CURVE ( 'NONE', #90740, #19180, #72359, .T. ) ;
#49575=CARTESIAN_POINT ( 'NONE',  ( -71.92287095715006728, -23.47593901973090169, -1.443836447538997536 ) ) ;
#49576=CARTESIAN_POINT ( 'NONE',  ( 13.31140876108729998, -18.89465134148960956, -1.500000000000002220 ) ) ;
#49577=CARTESIAN_POINT ( 'NONE',  ( -104.5154210034890951, -24.15620529776629155, 10.23563542870659759 ) ) ;
#49578=CARTESIAN_POINT ( 'NONE',  ( -11.21218820807429140, -16.99972530465495169, -1.500000000000002220 ) ) ;
#49579=EDGE_LOOP ( 'NONE', ( #79637, #33341, #83281, #87652 ) ) ;
#49580=CARTESIAN_POINT ( 'NONE',  ( -70.52590259285405239, -25.03444510360072783, 7.555793054676811060 ) ) ;
#49581=CARTESIAN_POINT ( 'NONE',  ( -29.54488130240525479, -24.07305817887745292, 10.23563548314527338 ) ) ;
#49582=CARTESIAN_POINT ( 'NONE',  ( -89.43576144935765626, -25.11033443737753501, 2.832404817301928723 ) ) ;
#49583=CARTESIAN_POINT ( 'NONE',  ( -70.52593452554701514, -25.25855380673795736, 7.557316893954395098 ) ) ;
#49584=ORIENTED_EDGE ( 'NONE', *, *, #42073, .F. ) ;
#49585=CARTESIAN_POINT ( 'NONE',  ( -29.00221282414159418, -24.76881061849349308, 3.230370487592436390 ) ) ;
#49586=CARTESIAN_POINT ( 'NONE',  ( -93.52287095715004739, -24.33927499327855770, 9.819080762295802955 ) ) ;
#49587=ORIENTED_EDGE ( 'NONE', *, *, #64031, .T. ) ;
#49588=B_SPLINE_CURVE_WITH_KNOTS ( 'NONE', 3,
 ( #40604, #88278, #63965, #17761, #63455, #72063 ),
 .UNSPECIFIED., .F., .F.,
 ( 4, 2, 4 ),
 ( 6.391158118961560919E-06, 0.001387004593080777906, 0.002767618028042594189 ),
 .UNSPECIFIED. ) ;
#49589=CARTESIAN_POINT ( 'NONE',  ( -7.357705842588929457, 19.43699106120834230, -1.500000000000002220 ) ) ;
#49591=ORIENTED_EDGE ( 'NONE', *, *, #54147, .F. ) ;
#49592=CARTESIAN_POINT ( 'NONE',  ( -125.5562618372648416, -23.85016227208582151, -0.8807180028928047744 ) ) ;
#49595=EDGE_CURVE ( 'NONE', #70388, #16861, #41996, .T. ) ;
#49597=CARTESIAN_POINT ( 'NONE',  ( -97.52287095715006160, -24.35013146730203815, 9.818937971375095941 ) ) ;
#49598=VERTEX_POINT ( 'NONE', #86231 ) ;
#49601=LINE ( 'NONE', #72931, #17055 ) ;
#49602=CARTESIAN_POINT ( 'NONE',  ( -98.58953762381672448, -23.48786465467241769, 11.44779295918254292 ) ) ;
#49604=CARTESIAN_POINT ( 'NONE',  ( -43.49278784741275672, -24.35071581493542681, 9.817618358456032368 ) ) ;
#49605=CARTESIAN_POINT ( 'NONE',  ( -21.42919730060085115, -5.301375089729956969, 11.49999999999999645 ) ) ;
#49606=ORIENTED_EDGE ( 'NONE', *, *, #80690, .F. ) ;
#49607=ADVANCED_FACE ( 'NONE', ( #2505 ), #55800, .T. ) ;
#49608=AXIS2_PLACEMENT_3D ( 'NONE', #59273, #5977, #5481 ) ;
#49610=CARTESIAN_POINT ( 'NONE',  ( -19.71520456405594857, 11.01310763156902972, -1.500000000000002220 ) ) ;
#49613=CARTESIAN_POINT ( 'NONE',  ( -127.6228709571500559, -29.50250786944525672, 11.44777988621622633 ) ) ;
#49614=ORIENTED_EDGE ( 'NONE', *, *, #84082, .F. ) ;
#49618=ORIENTED_EDGE ( 'NONE', *, *, #12814, .F. ) ;
#49619=CARTESIAN_POINT ( 'NONE',  ( -10.65520286329281596, -18.28862552182625123, 11.49999999999998934 ) ) ;
#49620=CARTESIAN_POINT ( 'NONE',  ( -78.94558681842012504, -25.03137978718093493, 6.087055896365015428 ) ) ;
#49622=CARTESIAN_POINT ( 'NONE',  ( -39.52287095715006870, -23.47593901973090524, -1.443836447538997092 ) ) ;
#49623=CARTESIAN_POINT ( 'NONE',  ( 2.725811458822067657, 22.07344620009914138, -1.500000000000002220 ) ) ;
#49624=CARTESIAN_POINT ( 'NONE',  ( -49.21454750704995007, -25.13941389702027251, 7.069183600260903866 ) ) ;
#49625=B_SPLINE_CURVE_WITH_KNOTS ( 'NONE', 3,
 ( #66618, #5184, #89923, #10805 ),
 .UNSPECIFIED., .F., .F.,
 ( 4, 4 ),
 ( 0.000000000000000000, 9.999999999998897304E-05 ),
 .UNSPECIFIED. ) ;
#49628=CARTESIAN_POINT ( 'NONE',  ( -37.47959251893834676, -24.65952944569304250, 1.056160979905692576 ) ) ;
#49629=CARTESIAN_POINT ( 'NONE',  ( -39.62287095715005592, -29.50250786944525672, 11.44777988621624232 ) ) ;
#49631=EDGE_CURVE ( 'NONE', #59549, #18030, #28670, .T. ) ;
#49632=CARTESIAN_POINT ( 'NONE',  ( 10.22484414329051994, 16.58839404647166660, -1.500000000000002220 ) ) ;
#49633=CARTESIAN_POINT ( 'NONE',  ( 9.988417798295188277, 18.97302403871600518, -1.500000000000002220 ) ) ;
#49636=CARTESIAN_POINT ( 'NONE',  ( -77.56399945295062537, -23.48783264082476663, -1.443836473390097241 ) ) ;
#49637=CARTESIAN_POINT ( 'NONE',  ( -7.601706241105644857, -21.46296766604531570, -1.500000000000002220 ) ) ;
#49638=EDGE_CURVE ( 'NONE', #12728, #19742, #51673, .T. ) ;
#49640=CARTESIAN_POINT ( 'NONE',  ( -98.58874431278923112, -24.34968618360934656, 0.1864209137778829184 ) ) ;
#49642=CARTESIAN_POINT ( 'NONE',  ( -11.57717615966994273, 16.22069937712612031, 11.49999999999999645 ) ) ;
#49643=CARTESIAN_POINT ( 'NONE',  ( -101.6228709571500985, -23.96177878511308990, 10.65340807706329507 ) ) ;
#49644=CARTESIAN_POINT ( 'NONE',  ( -39.58112737576117013, -24.51419770103158413, 9.386484678747189392 ) ) ;
#49645=CARTESIAN_POINT ( 'NONE',  ( -48.54086027304399664, -24.34968618360933945, 0.1864209137778883862 ) ) ;
#49647=CARTESIAN_POINT ( 'NONE',  ( -25.57928830845510504, -24.89106019490560229, 4.019483868920429082 ) ) ;
#49648=DIRECTION ( 'NONE',  ( -3.773278334453080206E-23, 0.9999999999976377785, 2.173523156925979975E-06 ) ) ;
#49649=CARTESIAN_POINT ( 'NONE',  ( 16.47784684176308545, -14.13017478139203220, -1.500000000000002220 ) ) ;
#49650=CARTESIAN_POINT ( 'NONE',  ( -51.92861116955014467, -25.24941396888022993, 6.270627690012409161 ) ) ;
#49651=CARTESIAN_POINT ( 'NONE',  ( 12.07855387261060898, -15.37489856218140183, -1.500000000000002220 ) ) ;
#49654=ORIENTED_EDGE ( 'NONE', *, *, #96170, .T. ) ;
#49656=CARTESIAN_POINT ( 'NONE',  ( -29.52287095715006160, -29.50250786944501158, 11.44777977277940550 ) ) ;
#49657=CARTESIAN_POINT ( 'NONE',  ( -16.05948562299510485, -12.68841425896798469, 11.49999999999999645 ) ) ;
#49658=CARTESIAN_POINT ( 'NONE',  ( -85.58953762381673869, -23.47593901973091235, -1.443836447539002865 ) ) ;
#49660=CARTESIAN_POINT ( 'NONE',  ( -39.62287095715006302, -24.33927499327853994, 9.819080762295820719 ) ) ;
#49663=CARTESIAN_POINT ( 'NONE',  ( -62.62287095715011986, -24.34917612406837861, 0.1852690917426612072 ) ) ;
#49671=CARTESIAN_POINT ( 'NONE',  ( -66.54900992194662024, -24.15620529776628089, 10.23563542870660470 ) ) ;
#49673=VECTOR ( 'NONE', #64278, 1000.000000000000114 ) ;
#49674=EDGE_CURVE ( 'NONE', #44036, #47480, #62645, .T. ) ;
#49675=CARTESIAN_POINT ( 'NONE',  ( 20.38051395842347802, -10.57019977742728578, 11.49999999999999645 ) ) ;
#49676=CARTESIAN_POINT ( 'NONE',  ( 6.135622925040504327, -21.92205258971886650, 11.49999999999998934 ) ) ;
#49677=CARTESIAN_POINT ( 'NONE',  ( -110.6272416013937629, -24.52399227489125266, 9.353111116836528183 ) ) ;
#49679=CARTESIAN_POINT ( 'NONE',  ( -90.62361245199505788, -25.00158670708910691, 2.256160236439220590 ) ) ;
#49681=CARTESIAN_POINT ( 'NONE',  ( -66.52287095715006160, -23.48783264082476663, -1.443836473390092134 ) ) ;
#49682=CARTESIAN_POINT ( 'NONE',  ( -70.26176671494545189, -25.13346133754408029, 7.099798033859436863 ) ) ;
#49683=CARTESIAN_POINT ( 'NONE',  ( -20.57654891367511851, 7.437132321665034240, -1.500000000000002220 ) ) ;
#49685=CARTESIAN_POINT ( 'NONE',  ( -26.65941713821050030, -24.79461012552177124, 2.761438400537009397 ) ) ;
#49687=CARTESIAN_POINT ( 'NONE',  ( -58.48922440719672977, -24.65952944569304606, 1.056160979905697461 ) ) ;
#49689=CARTESIAN_POINT ( 'NONE',  ( -6.584652030910324250, 19.34213596296284265, -1.500000000000002220 ) ) ;
#49690=ORIENTED_EDGE ( 'NONE', *, *, #30644, .F. ) ;
#49692=VERTEX_POINT ( 'NONE', #19207 ) ;
#49694=EDGE_CURVE ( 'NONE', #51872, #78417, #81115, .T. ) ;
#49695=CARTESIAN_POINT ( 'NONE',  ( -21.58539018223340022, -8.019882488244659768, -1.500000000000002220 ) ) ;
#49696=CARTESIAN_POINT ( 'NONE',  ( -105.5562042904834215, -23.48783264082478794, -1.443836473390059716 ) ) ;
#49697=CARTESIAN_POINT ( 'NONE',  ( -1.972954090310384379, -20.06304030521763337, -1.500000000000002220 ) ) ;
#49698=VERTEX_POINT ( 'NONE', #42572 ) ;
#49700=CARTESIAN_POINT ( 'NONE',  ( -67.62287095715004170, -24.51387760970723306, 9.387446482453416507 ) ) ;
#49702=ADVANCED_FACE ( 'NONE', ( #13086 ), #89732, .T. ) ;
#49703=B_SPLINE_CURVE_WITH_KNOTS ( 'NONE', 3,
 ( #98270, #21641, #4944, #29774, #51121, #58733 ),
 .UNSPECIFIED., .F., .F.,
 ( 4, 2, 4 ),
 ( 0.000000000000000000, 0.001380764517854758677, 0.002761529035709517355 ),
 .UNSPECIFIED. ) ;
#49705=CARTESIAN_POINT ( 'NONE',  ( -53.63875462047889187, -24.15620529776627734, 10.23563542870660825 ) ) ;
#49706=CARTESIAN_POINT ( 'NONE',  ( -19.99122433398336440, 7.574256484821010105, 11.49999999999999645 ) ) ;
#49709=CARTESIAN_POINT ( 'NONE',  ( -4.481184387785930312, -21.81124396384582909, 11.49999999999998934 ) ) ;
#49710=CARTESIAN_POINT ( 'NONE',  ( 18.97174343470660318, 8.267356841975738391, 11.49999999999998934 ) ) ;
#49711=EDGE_CURVE ( 'NONE', #8718, #11023, #52167, .T. ) ;
#49714=CARTESIAN_POINT ( 'NONE',  ( -70.79599823016188509, -25.03707830618030172, 7.590867772707287742 ) ) ;
#49716=LINE ( 'NONE', #9632, #51039 ) ;
#49717=ORIENTED_EDGE ( 'NONE', *, *, #48454, .F. ) ;
#49718=CARTESIAN_POINT ( 'NONE',  ( -111.3776484685884185, -25.28710546256126079, 4.332404433089555695 ) ) ;
#49719=CARTESIAN_POINT ( 'NONE',  ( -20.36979505965413395, -4.774807507659313721, -1.500000000000002220 ) ) ;
#49720=CARTESIAN_POINT ( 'NONE',  ( 16.40513048700843513, 14.50174154637248591, 11.49999999999999645 ) ) ;
#49722=FACE_OUTER_BOUND ( 'NONE', #96889, .T. ) ;
#49723=CARTESIAN_POINT ( 'NONE',  ( 19.74966320730700176, -10.79507447929251107, -1.500000000000002220 ) ) ;
#49724=CARTESIAN_POINT ( 'NONE',  ( 9.933205088616889000, -18.45388779576350302, 11.49999999999998934 ) ) ;
#49725=EDGE_CURVE ( 'NONE', #47965, #41069, #57794, .T. ) ;
#49726=CARTESIAN_POINT ( 'NONE',  ( -26.27733073949819698, -24.97067096850452472, 6.353770577458710989 ) ) ;
#49727=CARTESIAN_POINT ( 'NONE',  ( -108.8968792378191495, -25.09877477843093629, 7.294521336928838195 ) ) ;
#49729=ORIENTED_EDGE ( 'NONE', *, *, #28812, .T. ) ;
#49732=ORIENTED_EDGE ( 'NONE', *, *, #23866, .F. ) ;
#49733=CARTESIAN_POINT ( 'NONE',  ( -52.59912246993389573, -23.96119346886881019, -0.6495511937831939253 ) ) ;
#49734=VERTEX_POINT ( 'NONE', #12092 ) ;
#49736=CARTESIAN_POINT ( 'NONE',  ( 20.92345209525186078, -4.499874906010187026, -1.500000000000002220 ) ) ;
#49737=B_SPLINE_CURVE_WITH_KNOTS ( 'NONE', 3,
 ( #41652, #43146, #56885, #64510, #74092, #2588 ),
 .UNSPECIFIED., .F., .F.,
 ( 4, 2, 4 ),
 ( 0.000000000000000000, 0.001380901958385388761, 0.002761803916770777523 ),
 .UNSPECIFIED. ) ;
#49738=ORIENTED_EDGE ( 'NONE', *, *, #17308, .T. ) ;
#49739=CARTESIAN_POINT ( 'NONE',  ( -28.58953762381671737, -23.31699783904767287, 11.44779300560929514 ) ) ;
#49741=CARTESIAN_POINT ( 'NONE',  ( 18.35617536642501690, 10.39506492455470088, -1.500000000000002220 ) ) ;
#49742=CARTESIAN_POINT ( 'NONE',  ( -30.60105355972280350, -24.67579744659554208, 8.908675929220796874 ) ) ;
#49744=CARTESIAN_POINT ( 'NONE',  ( -43.52287095715006160, -23.47596703998600631, 11.44779298504229281 ) ) ;
#49745=VECTOR ( 'NONE', #91009, 1000.000000000000114 ) ;
#49746=CARTESIAN_POINT ( 'NONE',  ( -80.39981004835770761, -25.30877073141563827, 4.506608216669599543 ) ) ;
#49747=CARTESIAN_POINT ( 'NONE',  ( -129.5221660731197630, -23.73791477778912551, 11.05961554403170055 ) ) ;
#49748=CARTESIAN_POINT ( 'NONE',  ( -21.12052157030387889, 6.262089831203976331, -1.500000000000002220 ) ) ;
#49749=VERTEX_POINT ( 'NONE', #43062 ) ;
#49750=CARTESIAN_POINT ( 'NONE',  ( -65.58122294851770562, -24.83644354573579349, 8.397322867130094792 ) ) ;
#49751=DIRECTION ( 'NONE',  ( 3.773278334444166432E-23, -1.000000000000000000, 0.000000000000000000 ) ) ;
#49754=CARTESIAN_POINT ( 'NONE',  ( -28.40056905271415744, -24.97190405984839146, 2.662461283694066871 ) ) ;
#49757=CARTESIAN_POINT ( 'NONE',  ( 16.11712757473013014, 13.99349609535929773, -1.500000000000002220 ) ) ;
#49758=CARTESIAN_POINT ( 'NONE',  ( -70.43046027505549489, -25.31470333651159166, 4.855693143746263374 ) ) ;
#49759=CARTESIAN_POINT ( 'NONE',  ( -51.94816396996625940, -25.31392319263089519, 5.203681702801226550 ) ) ;
#49762=CARTESIAN_POINT ( 'NONE',  ( 14.20245820080859289, -17.52920931871068433, -1.500000000000002220 ) ) ;
#49764=ORIENTED_EDGE ( 'NONE', *, *, #77185, .F. ) ;
#49766=CARTESIAN_POINT ( 'NONE',  ( -79.50886169859143138, -24.15543982623907127, -0.2315651400026654261 ) ) ;
#49767=CARTESIAN_POINT ( 'NONE',  ( 18.87426695099163254, 5.791883100666666451, 11.49999999999999645 ) ) ;
#49768=CARTESIAN_POINT ( 'NONE',  ( -49.52287095715006870, -24.50216790748205398, 0.6166512839542435120 ) ) ;
#49771=CARTESIAN_POINT ( 'NONE',  ( -80.13654269935766195, -25.21083105912962097, 3.409327675794633361 ) ) ;
#49772=CARTESIAN_POINT ( 'NONE',  ( -29.81116077451118329, -24.60094588784620839, 4.841837093663297509 ) ) ;
#49773=CARTESIAN_POINT ( 'NONE',  ( -101.1944152955115044, -25.12268512865201586, 6.858246136620771871 ) ) ;
#49774=CARTESIAN_POINT ( 'NONE',  ( 2.580163054138214562, 21.43444414123800712, -1.500000000000002220 ) ) ;
#49776=CARTESIAN_POINT ( 'NONE',  ( -126.6228709571500559, -23.72773821059537269, 11.05748984161097681 ) ) ;
#49777=DIRECTION ( 'NONE',  ( -3.773278334444167608E-23, 1.000000000000000000, 0.000000000000000000 ) ) ;
#49779=LINE ( 'NONE', #12182, #15070 ) ;
#49780=CARTESIAN_POINT ( 'NONE',  ( 5.507670110241905448, 19.00313184189250038, 11.49999999999998934 ) ) ;
#49781=B_SPLINE_CURVE_WITH_KNOTS ( 'NONE', 3,
 ( #91292, #52241, #51235, #20267 ),
 .UNSPECIFIED., .F., .F.,
 ( 4, 4 ),
 ( 0.000000000000000000, 9.999999999997510880E-05 ),
 .UNSPECIFIED. ) ;
#49784=CARTESIAN_POINT ( 'NONE',  ( -15.67655817637044890, 12.86142704545212290, 11.49999999999999645 ) ) ;
#49788=CARTESIAN_POINT ( 'NONE',  ( -37.52287095715006870, -24.66019654487199375, 8.947790411086122830 ) ) ;
#49789=CARTESIAN_POINT ( 'NONE',  ( -51.52530242769704927, -25.25461990700743442, 6.116794828230213810 ) ) ;
#49791=EDGE_CURVE ( 'NONE', #64023, #43186, #25059, .T. ) ;
#49795=CARTESIAN_POINT ( 'NONE',  ( 19.36564117097816862, 5.170944958934900804, -1.500000000000002220 ) ) ;
#49798=VERTEX_POINT ( 'NONE', #39433 ) ;
#49799=EDGE_CURVE ( 'NONE', #74994, #97261, #806, .T. ) ;
#49804=CARTESIAN_POINT ( 'NONE',  ( -100.5562042904833788, -24.99156044556202261, 7.747789690856172307 ) ) ;
#49806=CARTESIAN_POINT ( 'NONE',  ( -73.52211523830358431, -23.48783264082477018, -1.443836473390094355 ) ) ;
#49808=CARTESIAN_POINT ( 'NONE',  ( -84.58953762381673869, -24.64898659630367561, 1.056161002820385164 ) ) ;
#49810=AXIS2_PLACEMENT_3D ( 'NONE', #2436, #9537, #41497 ) ;
#49811=CARTESIAN_POINT ( 'NONE',  ( 3.964343641299885146, 19.94596313931659992, -1.500000000000002220 ) ) ;
#49813=B_SPLINE_CURVE_WITH_KNOTS ( 'NONE', 3,
 ( #82603, #68877, #76475, #45057 ),
 .UNSPECIFIED., .F., .F.,
 ( 4, 4 ),
 ( 0.000000000000000000, 0.002094050480769216183 ),
 .UNSPECIFIED. ) ;
#49815=CARTESIAN_POINT ( 'NONE',  ( -16.74478417649319084, -15.65585335247391896, -1.500000000000002220 ) ) ;
#49817=CARTESIAN_POINT ( 'NONE',  ( -122.5228709571501042, -24.51283580621365132, 0.6167428607019895814 ) ) ;
#49818=EDGE_LOOP ( 'NONE', ( #59705, #55075, #20777, #52473 ) ) ;
#49819=B_SPLINE_CURVE_WITH_KNOTS ( 'NONE', 3,
 ( #22961, #60075, #83883, #69672, #7761, #53954 ),
 .UNSPECIFIED., .F., .F.,
 ( 4, 2, 4 ),
 ( 0.000000000000000000, 0.001380764517853251853, 0.002761529035706503706 ),
 .UNSPECIFIED. ) ;
#49820=DIRECTION ( 'NONE',  ( 3.773278334444167608E-23, -1.000000000000000000, 0.000000000000000000 ) ) ;
#49821=CARTESIAN_POINT ( 'NONE',  ( -50.04767967325393840, -25.26264170184645508, 7.063298022568840651 ) ) ;
#49822=EDGE_CURVE ( 'NONE', #96700, #79877, #84362, .T. ) ;
#49823=CARTESIAN_POINT ( 'NONE',  ( -30.47287095715007865, -24.75746604436832499, 8.625480456497754744 ) ) ;
#49824=CARTESIAN_POINT ( 'NONE',  ( 13.39648796734645231, 16.42122281929413319, 11.49999999999999645 ) ) ;
#49825=CARTESIAN_POINT ( 'NONE',  ( 19.81268554055766273, 9.900562300003143079, 11.49999999999998934 ) ) ;
#49826=CARTESIAN_POINT ( 'NONE',  ( 13.11803791274172681, -15.88952355948706341, -1.500000000000002220 ) ) ;
#49828=CARTESIAN_POINT ( 'NONE',  ( -111.5562042904833930, -23.48783264082479150, -1.443836473390061492 ) ) ;
#49830=CARTESIAN_POINT ( 'NONE',  ( -54.61288136965932694, -23.48783264082476308, -1.443836473390098130 ) ) ;
#49832=EDGE_LOOP ( 'NONE', ( #2772, #58766, #49501, #53708 ) ) ;
#49833=VERTEX_POINT ( 'NONE', #25572 ) ;
#49835=CARTESIAN_POINT ( 'NONE',  ( -83.62287095715004170, -23.73907113216991860, -1.053371485793229256 ) ) ;
#49836=CARTESIAN_POINT ( 'NONE',  ( -28.51174970316478863, -23.57371711286328519, 11.05961558438220926 ) ) ;
#49837=CARTESIAN_POINT ( 'NONE',  ( -109.3584176993576591, -29.50249212968922308, 4.206193347771797875 ) ) ;
#49838=CARTESIAN_POINT ( 'NONE',  ( -14.21563987850626276, 15.01860006206015008, -1.500000000000002220 ) ) ;
#49839=CARTESIAN_POINT ( 'NONE',  ( 21.40858030128615397, -3.853468400179685727, 11.49999999999999645 ) ) ;
#49840=ORIENTED_EDGE ( 'NONE', *, *, #78833, .F. ) ;
#49841=CARTESIAN_POINT ( 'NONE',  ( -62.55620429048339304, -24.65952944569304606, 1.056160979905697905 ) ) ;
#49842=CARTESIAN_POINT ( 'NONE',  ( -75.52287095715011844, -23.48783264082477373, -1.443836473390087694 ) ) ;
#49843=CARTESIAN_POINT ( 'NONE',  ( 5.309366582633749054, -21.77581755331916824, -1.500000000000002220 ) ) ;
#49847=VERTEX_POINT ( 'NONE', #48925 ) ;
#49850=B_SPLINE_SURFACE_WITH_KNOTS ( 'NONE', 3, 3, ( 
 ( #34408, #96304, #56766, #81080 ),
 ( #4466, #49644, #12054, #73470 ),
 ( #18179, #41525, #27295, #26295 ),
 ( #66374, #57270, #42035, #72980 ),
 ( #49154, #65387, #80079, #10563 ),
 ( #34907, #19664, #35416, #97303 ),
 ( #59243, #21651, #20663, #97792 ) ),
 .UNSPECIFIED., .F., .F., .F.,
 ( 4, 3, 4 ),
 ( 4, 4 ),
 ( 0.7945040050992251413, 0.8970133687736508987, 0.9995227324480766562 ),
 ( 0.9097251710157197024, 0.9111578850782391381 ),
 .UNSPECIFIED. ) ;
#49853=ORIENTED_EDGE ( 'NONE', *, *, #29330, .T. ) ;
#49855=LINE ( 'NONE', #66588, #78151 ) ;
#49856=ORIENTED_EDGE ( 'NONE', *, *, #24832, .T. ) ;
#49857=B_SPLINE_CURVE_WITH_KNOTS ( 'NONE', 3,
 ( #35989, #43611, #19259, #52224 ),
 .UNSPECIFIED., .F., .F.,
 ( 4, 4 ),
 ( 0.000000000000000000, 9.999999999998206125E-05 ),
 .UNSPECIFIED. ) ;
#49858=CARTESIAN_POINT ( 'NONE',  ( -17.78888362263414535, -11.56919986243916654, -1.500000000000002220 ) ) ;
#49859=VERTEX_POINT ( 'NONE', #18956 ) ;
#49860=CARTESIAN_POINT ( 'NONE',  ( -88.62596719604175632, -24.51314013834316086, 0.6176544820404141767 ) ) ;
#49861=CARTESIAN_POINT ( 'NONE',  ( 21.83686239284238084, -0.8075297431944471471, -1.500000000000002220 ) ) ;
#49862=CARTESIAN_POINT ( 'NONE',  ( -103.6250708163186118, -24.51419770103158058, 9.386484678747171628 ) ) ;
#49863=LINE ( 'NONE', #67082, #55003 ) ;
#49864=CARTESIAN_POINT ( 'NONE',  ( -111.7814946224345789, -25.28710546256127145, 4.332404433089555695 ) ) ;
#49865=CARTESIAN_POINT ( 'NONE',  ( -21.47987282208850601, -4.139150239982721580, -1.500000000000002220 ) ) ;
#49867=ORIENTED_EDGE ( 'NONE', *, *, #51790, .F. ) ;
#49868=PLANE ( 'NONE',  #76111 ) ;
#49869=CARTESIAN_POINT ( 'NONE',  ( -49.06509223983938739, -25.12782660346821828, 6.860564634149458385 ) ) ;
#49873=ORIENTED_EDGE ( 'NONE', *, *, #41493, .T. ) ;
#49874=DIRECTION ( 'NONE',  ( -3.773278334453079030E-23, 0.9999999999976377785, 2.173523156925979128E-06 ) ) ;
#49875=CARTESIAN_POINT ( 'NONE',  ( -10.25850006537117487, -22.80581235653748706, 0.3010598746230520595 ) ) ;
#49876=CARTESIAN_POINT ( 'NONE',  ( -19.44786352930952233, -8.617208915446557427, 11.49999999999998934 ) ) ;
#49879=FACE_OUTER_BOUND ( 'NONE', #95131, .T. ) ;
#49881=CARTESIAN_POINT ( 'NONE',  ( -84.62287095715008434, -23.96177878511308634, 10.65340807706329862 ) ) ;
#49882=CARTESIAN_POINT ( 'NONE',  ( -19.27395093635484713, 2.380100695660296140, -1.500000000000002220 ) ) ;
#49883=CARTESIAN_POINT ( 'NONE',  ( -117.5162819473935372, -24.66019654487200441, 8.947790411086112172 ) ) ;
#49885=CARTESIAN_POINT ( 'NONE',  ( 18.72186718581493636, -5.619560887262019300, 11.49999999999999645 ) ) ;
#49888=CARTESIAN_POINT ( 'NONE',  ( -116.5562042904833930, -23.48786465467241769, 11.44779295918253759 ) ) ;
#49890=CARTESIAN_POINT ( 'NONE',  ( -97.62287095715004170, -23.72747288104441665, -1.053458166803661111 ) ) ;
#49891=CARTESIAN_POINT ( 'NONE',  ( -89.55819824587750588, -23.73766607897671221, -1.055555164236434473 ) ) ;
#49892=DIRECTION ( 'NONE',  ( -1.000000000000000000, -3.773278334444167608E-23, -8.201307833595939069E-29 ) ) ;
#49893=CARTESIAN_POINT ( 'NONE',  ( -81.83126432988071031, -25.24813773485163537, 6.560967144104515647 ) ) ;
#49894=CARTESIAN_POINT ( 'NONE',  ( -9.385407830382300531, 17.29636241635495608, -1.500000000000002220 ) ) ;
#49896=B_SPLINE_CURVE_WITH_KNOTS ( 'NONE', 3,
 ( #29905, #13173, #67987, #75074, #28911, #60873 ),
 .UNSPECIFIED., .F., .F.,
 ( 4, 2, 4 ),
 ( 1.570755371633856203E-05, 0.001396183895866086452, 0.002776660238015834278 ),
 .UNSPECIFIED. ) ;
#49897=CARTESIAN_POINT ( 'NONE',  ( -78.52287095715006160, -24.34917612406837151, 0.1852690917426541017 ) ) ;
#49898=CARTESIAN_POINT ( 'NONE',  ( -77.62287095715005592, -29.50250243563736774, 8.947779886222141599 ) ) ;
#49900=ORIENTED_EDGE ( 'NONE', *, *, #58488, .T. ) ;
#49901=DIRECTION ( 'NONE',  ( -3.773278334453079618E-23, 0.9999999999976377785, 2.173523156925979975E-06 ) ) ;
#49902=CARTESIAN_POINT ( 'NONE',  ( -105.6228709571499991, -24.51254535404256885, 9.355368623467647637 ) ) ;
#49903=CARTESIAN_POINT ( 'NONE',  ( -47.52204414629284202, -23.48783264082478084, -1.443836473390071706 ) ) ;
#49904=CARTESIAN_POINT ( 'NONE',  ( -83.62287095715005592, -29.50248528299804818, 1.056150453629038477 ) ) ;
#49905=CARTESIAN_POINT ( 'NONE',  ( -78.92501255663768234, -25.29489613318244068, 6.057562805997258160 ) ) ;
#49906=EDGE_CURVE ( 'NONE', #53781, #80749, #93207, .T. ) ;
#49907=CARTESIAN_POINT ( 'NONE',  ( -109.6228709571500559, -23.47596703998600631, 11.44779298504227860 ) ) ;
#49909=CARTESIAN_POINT ( 'NONE',  ( -4.495603250223349612, -19.44740727768710187, 11.49999999999998934 ) ) ;
#49910=EDGE_CURVE ( 'NONE', #72067, #9106, #10520, .T. ) ;
#49911=CARTESIAN_POINT ( 'NONE',  ( -0.08481413156557598976, -21.95201441650188201, 10.11439756690867320 ) ) ;
#49912=CARTESIAN_POINT ( 'NONE',  ( 18.06118663784855372, 8.336529998961283994, -1.500000000000002220 ) ) ;
#49913=VERTEX_POINT ( 'NONE', #61782 ) ;
#49915=CARTESIAN_POINT ( 'NONE',  ( -56.52287095715006870, -24.65952944569304606, 1.056160979905695463 ) ) ;
#49916=EDGE_CURVE ( 'NONE', #58574, #61812, #23692, .T. ) ;
#49917=B_SPLINE_CURVE_WITH_KNOTS ( 'NONE', 3,
 ( #6913, #76908, #86037, #99739 ),
 .UNSPECIFIED., .F., .F.,
 ( 4, 4 ),
 ( 0.000000000000000000, 9.999999999997510880E-05 ),
 .UNSPECIFIED. ) ;
#49918=EDGE_CURVE ( 'NONE', #23306, #16634, #16626, .T. ) ;
#49921=CARTESIAN_POINT ( 'NONE',  ( 7.312689604342500260, -19.48077458720139532, 11.49999999999999645 ) ) ;
#49923=EDGE_CURVE ( 'NONE', #25116, #66785, #85099, .T. ) ;
#49924=CARTESIAN_POINT ( 'NONE',  ( -62.58953762381673158, -23.47596703998600276, 11.44779298504227505 ) ) ;
#49925=CARTESIAN_POINT ( 'NONE',  ( 10.78062712001149492, -20.16176685268226976, 11.49999999999999645 ) ) ;
#49927=B_SPLINE_SURFACE_WITH_KNOTS ( 'NONE', 3, 3, ( 
 ( #79577, #26296, #58741, #73471 ),
 ( #50630, #57271, #66867, #90186 ),
 ( #4467, #88201, #57757, #35899 ),
 ( #3966, #13050, #34409, #27296 ),
 ( #18671, #64890, #49645, #35417 ),
 ( #97793, #58253, #65389, #95800 ),
 ( #72480, #28284, #80577, #89196 ) ),
 .UNSPECIFIED., .F., .F., .F.,
 ( 4, 3, 4 ),
 ( 4, 4 ),
 ( 0.0004766839783839649258, 0.1029713700210903998, 0.2054660560637968370 ),
 ( 0.8197025155639751093, 0.8210934493545416490 ),
 .UNSPECIFIED. ) ;
#49928=CARTESIAN_POINT ( 'NONE',  ( -64.62287095715008434, -24.51283580621364422, 0.6167428607019749265 ) ) ;
#49929=CARTESIAN_POINT ( 'NONE',  ( -92.52287095715006160, -23.95044443724992078, 10.65354141964649237 ) ) ;
#49930=EDGE_LOOP ( 'NONE', ( #70204, #30541, #21949, #48319 ) ) ;
#49931=CARTESIAN_POINT ( 'NONE',  ( -13.58233929615340152, 14.99024694321910900, -1.500000000000002220 ) ) ;
#49932=B_SPLINE_CURVE_WITH_KNOTS ( 'NONE', 3,
 ( #68772, #29210, #91597, #30700 ),
 .UNSPECIFIED., .F., .F.,
 ( 4, 4 ),
 ( 0.000000000000000000, 1.000000000000000000 ),
 .UNSPECIFIED. ) ;
#49934=PLANE ( 'NONE',  #27470 ) ;
#49935=AXIS2_PLACEMENT_3D ( 'NONE', #61745, #39389, #92169 ) ;
#49936=DIRECTION ( 'NONE',  ( -3.773278334453079030E-23, 0.9999999999976377785, 2.173523156925979128E-06 ) ) ;
#49937=ORIENTED_EDGE ( 'NONE', *, *, #41195, .T. ) ;
#49938=CARTESIAN_POINT ( 'NONE',  ( -106.2228709571500787, -23.47596703998600631, 11.44779298504227860 ) ) ;
#49939=CARTESIAN_POINT ( 'NONE',  ( -100.6228709571500275, -24.82558206586150007, 1.605769216559626233 ) ) ;
#49940=CARTESIAN_POINT ( 'NONE',  ( 13.83478396660306942, -14.44641118834825910, -1.500000000000002220 ) ) ;
#49941=CARTESIAN_POINT ( 'NONE',  ( -20.94189920129180038, 1.864940847883316488, 11.49999999999999645 ) ) ;
#49944=CARTESIAN_POINT ( 'NONE',  ( 21.84380375219137349, -3.031640915038902762, 11.49999999999998934 ) ) ;
#49946=CARTESIAN_POINT ( 'NONE',  ( -39.54917078480641379, -25.27806004098935233, 4.610327274970852152 ) ) ;
#49947=DIRECTION ( 'NONE',  ( -3.773278334453079030E-23, 0.9999999999976377785, 2.173523156925979128E-06 ) ) ;
#49948=FACE_OUTER_BOUND ( 'NONE', #15939, .T. ) ;
#49949=CARTESIAN_POINT ( 'NONE',  ( -72.58096839274725198, -24.65952944569304250, 1.056160979905695463 ) ) ;
#49950=DIRECTION ( 'NONE',  ( 0.000000000000000000, -2.173523156925980399E-06, 0.9999999999976378895 ) ) ;
#49951=ORIENTED_EDGE ( 'NONE', *, *, #6224, .F. ) ;
#49953=B_SPLINE_CURVE_WITH_KNOTS ( 'NONE', 3,
 ( #45163, #76087, #6585, #37540, #29919, #60886, #32426, #86211 ),
 .UNSPECIFIED., .F., .F.,
 ( 4, 2, 2, 4 ),
 ( -0.001240355328176894791, -0.0002398155169399769290, 0.0007607242942969409324, 0.002761803916770776655 ),
 .UNSPECIFIED. ) ;
#49954=ORIENTED_EDGE ( 'NONE', *, *, #7663, .F. ) ;
#49957=FACE_OUTER_BOUND ( 'NONE', #90111, .T. ) ;
#49958=CARTESIAN_POINT ( 'NONE',  ( -10.66544979547405347, 17.54311462378693420, -1.500000000000002220 ) ) ;
#49959=ORIENTED_EDGE ( 'NONE', *, *, #13406, .T. ) ;
#49963=CARTESIAN_POINT ( 'NONE',  ( -21.99995728619510516, 3.820703864638951952, 11.49999999999998934 ) ) ;
#49965=CARTESIAN_POINT ( 'NONE',  ( -31.62287095715005236, -23.48783264082477729, -1.443836473390074149 ) ) ;
#49966=ORIENTED_EDGE ( 'NONE', *, *, #93990, .T. ) ;
#49967=CARTESIAN_POINT ( 'NONE',  ( -31.24388727629348494, -24.86181185134534388, 1.747789972853592610 ) ) ;
#49970=CARTESIAN_POINT ( 'NONE',  ( -6.911038104174170194, -19.68591361114308214, -1.500000000000002220 ) ) ;
#49972=EDGE_CURVE ( 'NONE', #48183, #90746, #98566, .T. ) ;
#49973=CARTESIAN_POINT ( 'NONE',  ( -39.22702504168157134, -25.21450095976316064, 3.515138031494141835 ) ) ;
#49975=ORIENTED_EDGE ( 'NONE', *, *, #76568, .F. ) ;
#49976=CARTESIAN_POINT ( 'NONE',  ( -68.94461706535129508, -25.03149113892856192, 6.371760577998683672 ) ) ;
#49977=CARTESIAN_POINT ( 'NONE',  ( -8.250207518706217158, 19.40231308534122689, -1.500000000000002220 ) ) ;
#49978=EDGE_CURVE ( 'NONE', #9703, #51976, #60034, .T. ) ;
#49980=LINE ( 'NONE', #66210, #54370 ) ;
#49982=CARTESIAN_POINT ( 'NONE',  ( -120.5526909221348575, -24.83644354573579349, 8.397322867130096569 ) ) ;
#49983=DIRECTION ( 'NONE',  ( 0.000000000000000000, -0.9999999999976377785, -2.173523156925979128E-06 ) ) ;
#49985=CARTESIAN_POINT ( 'NONE',  ( -21.46818342838279392, -2.986162219498790904, -1.500000000000002220 ) ) ;
#49986=CARTESIAN_POINT ( 'NONE',  ( -81.45245898465185519, -25.24759656628838655, 6.419335927061524671 ) ) ;
#49987=CARTESIAN_POINT ( 'NONE',  ( 6.060481786824854389, 21.40074245971799627, 11.49999999999999645 ) ) ;
#49988=EDGE_LOOP ( 'NONE', ( #85399, #70697, #52955, #81992 ) ) ;
#49989=CARTESIAN_POINT ( 'NONE',  ( -72.62287095715007013, -24.35013146730203815, 9.818937971375111928 ) ) ;
#49994=ORIENTED_EDGE ( 'NONE', *, *, #21002, .T. ) ;
#49998=DIRECTION ( 'NONE',  ( 3.773278334444166432E-23, -1.000000000000000000, 0.000000000000000000 ) ) ;
#50000=ORIENTED_EDGE ( 'NONE', *, *, #81833, .F. ) ;
#50001=CARTESIAN_POINT ( 'NONE',  ( -130.5728709571500872, -24.99287569232926387, 8.157771170601387567 ) ) ;
#50002=CARTESIAN_POINT ( 'NONE',  ( -16.74552829020559130, -14.98668287627115170, -1.500000000000002220 ) ) ;
#50003=ORIENTED_EDGE ( 'NONE', *, *, #54781, .F. ) ;
#50004=CARTESIAN_POINT ( 'NONE',  ( -99.68246233598412687, -25.07904460479134912, 7.390530277590735331 ) ) ;
#50005=CARTESIAN_POINT ( 'NONE',  ( -101.6314124882551795, -23.96169478059713853, 10.65365249895717881 ) ) ;
#50009=CARTESIAN_POINT ( 'NONE',  ( -97.24791950549985131, -24.66459861931856778, 1.095224832288509198 ) ) ;
#50010=CARTESIAN_POINT ( 'NONE',  ( 19.59400933563812330, 0.1774559437341752532, -1.500000000000002220 ) ) ;
#50011=CARTESIAN_POINT ( 'NONE',  ( -59.52287095715006160, -24.65952944569304961, 1.056160979905695463 ) ) ;
#50012=VERTEX_POINT ( 'NONE', #51417 ) ;
#50013=B_SPLINE_CURVE_WITH_KNOTS ( 'NONE', 3,
 ( #9539, #94772, #40500, #1942, #63858, #25260, #56239, #13895 ),
 .UNSPECIFIED., .F., .F.,
 ( 4, 2, 2, 4 ),
 ( 0.000000000000000000, 0.002001098010032680181, 0.003001647015049020272, 0.004002196020065360363 ),
 .UNSPECIFIED. ) ;
#50014=CARTESIAN_POINT ( 'NONE',  ( -21.28347836979250118, 3.227085873532868021, 11.49999999999998934 ) ) ;
#50016=CARTESIAN_POINT ( 'NONE',  ( -81.42380231474228935, -25.31572696169300585, 5.197788986266723477 ) ) ;
#50017=CARTESIAN_POINT ( 'NONE',  ( -63.62287095715004881, -24.65952944569303895, 1.056160979905696129 ) ) ;
#50019=CARTESIAN_POINT ( 'NONE',  ( -12.88233675513024856, -19.01995677650982230, -1.500000000000002220 ) ) ;
#50021=CARTESIAN_POINT ( 'NONE',  ( -92.62287095715005592, -23.47593901973091235, -1.443836447539002865 ) ) ;
#50022=FACE_OUTER_BOUND ( 'NONE', #78005, .T. ) ;
#50023=CARTESIAN_POINT ( 'NONE',  ( 18.22116949570664701, -8.484823103377051368, 11.49999999999999645 ) ) ;
#50026=VECTOR ( 'NONE', #73994, 1000.000000000000227 ) ;
#50027=CARTESIAN_POINT ( 'NONE',  ( -98.62287095715005592, -29.50248528299804818, 1.056150453629042030 ) ) ;
#50029=CARTESIAN_POINT ( 'NONE',  ( -126.6228709571500559, -24.64965695001469825, 8.947790433994173398 ) ) ;
#50030=CARTESIAN_POINT ( 'NONE',  ( 16.83370257367741019, -10.51912618480096206, 11.49999999999998934 ) ) ;
#50031=LINE ( 'NONE', #55642, #43125 ) ;
#50032=CARTESIAN_POINT ( 'NONE',  ( 6.816645498261984848, 18.52099371530728789, -1.500000000000002220 ) ) ;
#50033=CARTESIAN_POINT ( 'NONE',  ( -42.56072380411180944, -23.73766607897670156, -1.055555164236442689 ) ) ;
#50037=CARTESIAN_POINT ( 'NONE',  ( -115.6228709571499706, -24.14321612903118108, -0.2833117244521116684 ) ) ;
#50039=CARTESIAN_POINT ( 'NONE',  ( 6.226698476505521995, -19.64469265145860177, 11.49999999999999645 ) ) ;
#50040=EDGE_CURVE ( 'NONE', #11737, #24496, #55280, .T. ) ;
#50041=DIRECTION ( 'NONE',  ( 0.000000000000000000, -0.9999999999976377785, -2.173523156925979975E-06 ) ) ;
#50042=CARTESIAN_POINT ( 'NONE',  ( -2.919094682108430483, 22.50186656173435296, 11.49999999999999645 ) ) ;
#50043=ORIENTED_EDGE ( 'NONE', *, *, #68339, .T. ) ;
#50044=CARTESIAN_POINT ( 'NONE',  ( -69.70298246041917878, -25.25639558095986459, 6.901994508171235942 ) ) ;
#50045=CARTESIAN_POINT ( 'NONE',  ( -50.44230859488045127, -25.31264664644561435, 4.735025439241685952 ) ) ;
#50046=ADVANCED_FACE ( 'NONE', ( #90962 ), #74247, .T. ) ;
#50047=CARTESIAN_POINT ( 'NONE',  ( -111.3758965426668084, -25.18392475019902577, 6.830256960825760615 ) ) ;
#50048=CARTESIAN_POINT ( 'NONE',  ( -80.96226385320382235, -29.50248939449842922, 2.947779886236309377 ) ) ;
#50049=ORIENTED_EDGE ( 'NONE', *, *, #1362, .F. ) ;
#50051=CARTESIAN_POINT ( 'NONE',  ( -9.520747347383798243, -20.79447232172871907, 11.49999999999998934 ) ) ;
#50052=CARTESIAN_POINT ( 'NONE',  ( -98.58953762381672448, -24.64965694238407323, 8.947790433994651238 ) ) ;
#50054=LINE ( 'NONE', #15458, #92194 ) ;
#50055=CARTESIAN_POINT ( 'NONE',  ( -17.96456891314058879, -13.58578184957126034, 11.49999999999999645 ) ) ;
#50056=EDGE_LOOP ( 'NONE', ( #97001, #21815, #88248, #9532 ) ) ;
#50058=CARTESIAN_POINT ( 'NONE',  ( 21.77894307773758698, -2.757304969434911879, -1.500000000000002220 ) ) ;
#50059=CARTESIAN_POINT ( 'NONE',  ( -111.5501966621663996, -24.65952944569305316, 1.056160979905705677 ) ) ;
#50060=CARTESIAN_POINT ( 'NONE',  ( -29.17238308422418669, -25.21724654464993520, 6.041339601850384433 ) ) ;
#50061=ORIENTED_EDGE ( 'NONE', *, *, #61263, .F. ) ;
#50062=DIRECTION ( 'NONE',  ( -1.000000000000000000, -3.773278334444166432E-23, -8.201307841325785021E-29 ) ) ;
#50063=PLANE ( 'NONE',  #7337 ) ;
#50065=CARTESIAN_POINT ( 'NONE',  ( -49.52287095715006160, -23.48786465467241769, 11.44779295918255002 ) ) ;
#50066=VECTOR ( 'NONE', #68011, 1000.000000000000114 ) ;
#50067=CARTESIAN_POINT ( 'NONE',  ( 18.14102482237423075, -9.550406459077080967, 11.49999999999998934 ) ) ;
#50068=ORIENTED_EDGE ( 'NONE', *, *, #61593, .T. ) ;
#50070=ORIENTED_EDGE ( 'NONE', *, *, #40634, .F. ) ;
#50073=CARTESIAN_POINT ( 'NONE',  ( 1.702247502073919394, 23.03039350466679025, -1.500000000000002220 ) ) ;
#50074=CARTESIAN_POINT ( 'NONE',  ( -102.5228709571500758, -29.50247984919015209, -1.443849546365050029 ) ) ;
#50075=CARTESIAN_POINT ( 'NONE',  ( -19.47531982339030776, -5.969937916086089480, -1.500000000000002220 ) ) ;
#50076=ORIENTED_EDGE ( 'NONE', *, *, #2463, .T. ) ;
#50079=CARTESIAN_POINT ( 'NONE',  ( -51.64970124796896300, -25.24249896790658454, 3.668597825874434282 ) ) ;
#50081=CARTESIAN_POINT ( 'NONE',  ( -105.6281938531929256, -24.52300882791530157, 0.6510814631126371488 ) ) ;
#50084=CARTESIAN_POINT ( 'NONE',  ( -29.24577077129365321, -25.21532183541616590, 4.691558442423485076 ) ) ;
#50086=ORIENTED_EDGE ( 'NONE', *, *, #98592, .T. ) ;
#50087=VECTOR ( 'NONE', #44795, 1000.000000000000114 ) ;
#50088=CARTESIAN_POINT ( 'NONE',  ( -18.04518632387085830, 10.29925911722504317, 11.49999999999998934 ) ) ;
#50089=ORIENTED_EDGE ( 'NONE', *, *, #63878, .T. ) ;
#50091=CARTESIAN_POINT ( 'NONE',  ( -40.35516601162786543, -25.30533514595981970, 5.080719793522692207 ) ) ;
#50094=CARTESIAN_POINT ( 'NONE',  ( -51.76227918482971546, -25.29444715957360756, 5.533495090563274488 ) ) ;
#50098=CARTESIAN_POINT ( 'NONE',  ( -68.62287095715005592, -24.35013146730203459, 9.818937971375113705 ) ) ;
#50099=CARTESIAN_POINT ( 'NONE',  ( -43.60778276898914640, -23.73791477778911130, 11.05961554403171121 ) ) ;
#50100=CARTESIAN_POINT ( 'NONE',  ( 17.94654606563480215, 12.89224558282342947, 11.49999999999999645 ) ) ;
#50102=CARTESIAN_POINT ( 'NONE',  ( -103.6308616004146330, -23.96119346886881019, -0.6495511937832079141 ) ) ;
#50103=CARTESIAN_POINT ( 'NONE',  ( -3.801653518169780366, -22.29579330195574016, -1.500000000000002220 ) ) ;
#50104=CARTESIAN_POINT ( 'NONE',  ( -99.22737670894692030, -25.30351348175197046, 5.230124031126243800 ) ) ;
#50105=ORIENTED_EDGE ( 'NONE', *, *, #66935, .T. ) ;
#50106=B_SPLINE_CURVE_WITH_KNOTS ( 'NONE', 3,
 ( #58102, #12888, #51474, #65721, #20502, #59592 ),
 .UNSPECIFIED., .F., .F.,
 ( 4, 2, 4 ),
 ( 0.000000000000000000, 0.001380901958385394833, 0.002761803916770789666 ),
 .UNSPECIFIED. ) ;
#50107=ORIENTED_EDGE ( 'NONE', *, *, #97294, .T. ) ;
#50111=CARTESIAN_POINT ( 'NONE',  ( -128.5895376238167103, -23.48783264082479505, -1.443836473390056829 ) ) ;
#50113=CARTESIAN_POINT ( 'NONE',  ( -7.741094375770895653, -19.69850519626218599, 11.49999999999998934 ) ) ;
#50115=DIRECTION ( 'NONE',  ( -3.773278334453080206E-23, 0.9999999999976377785, 2.173523156925979552E-06 ) ) ;
#50116=CARTESIAN_POINT ( 'NONE',  ( 13.76814385225720372, 17.53657229028232223, -1.500000000000002220 ) ) ;
#50124=B_SPLINE_CURVE_WITH_KNOTS ( 'NONE', 3,
 ( #37494, #36489, #14143, #67958, #20756, #84662, #76534, #67454, #98885, #98380, #5046, #75538, #22748, #90784 ),
 .UNSPECIFIED., .F., .F.,
 ( 4, 2, 2, 2, 2, 2, 4 ),
 ( 1.404617285391336434E-17, 0.0002430483912727410896, 0.0004860967825454681388, 0.0009721935650909229419, 0.001458290347636377691, 0.001701338738909113739, 0.001944387130181849570 ),
 .UNSPECIFIED. ) ;
#50125=CARTESIAN_POINT ( 'NONE',  ( -7.634514033349506512, -17.95459398628807435, 11.49999999999998934 ) ) ;
#50126=CARTESIAN_POINT ( 'NONE',  ( 18.57079561221590325, -10.74342183689097574, -1.500000000000002220 ) ) ;
#50129=PLANE ( 'NONE',  #58758 ) ;
#50130=CARTESIAN_POINT ( 'NONE',  ( -22.67762270672801250, 1.536325718666671225, -1.500000000000002220 ) ) ;
#50132=CARTESIAN_POINT ( 'NONE',  ( -98.62981750425619509, -24.15543982623907837, -0.2315651400026625395 ) ) ;
#50134=CARTESIAN_POINT ( 'NONE',  ( -18.10700488460823721, -8.296952762055457953, 11.49999999999999645 ) ) ;
#50135=CARTESIAN_POINT ( 'NONE',  ( -104.5573922166538665, -23.73766607897670866, -1.055555164236449572 ) ) ;
#50137=CARTESIAN_POINT ( 'NONE',  ( -42.62287095715004881, -23.48783264082477373, -1.443836473390072817 ) ) ;
#50138=B_SPLINE_CURVE_WITH_KNOTS ( 'NONE', 3,
 ( #71112, #25428, #72119, #94433, #1601, #86327, #63010, #2609, #16811, #33045, #26442, #79207, #49789, #24920 ),
 .UNSPECIFIED., .F., .F.,
 ( 4, 2, 2, 2, 2, 2, 4 ),
 ( 0.000000000000000000, 0.0002092458945023362355, 0.0004184917890046724711, 0.0008369835780093458095, 0.001255475367014019256, 0.001464721261516361509, 0.001673967156018703979 ),
 .UNSPECIFIED. ) ;
#50139=CARTESIAN_POINT ( 'NONE',  ( -76.62287095715007013, -23.47596703998600631, 11.44779298504227860 ) ) ;
#50142=PLANE ( 'NONE',  #93135 ) ;
#50144=CARTESIAN_POINT ( 'NONE',  ( -10.76533847658563126, -18.86179312034942868, -1.500000000000002220 ) ) ;
#50145=CARTESIAN_POINT ( 'NONE',  ( -51.93008509245395032, -25.25437732972921268, 6.222362237587184985 ) ) ;
#50147=CARTESIAN_POINT ( 'NONE',  ( -14.81708852449743929, -12.69844354874750181, -1.500000000000002220 ) ) ;
#50152=LINE ( 'NONE', #11080, #71077 ) ;
#50153=CARTESIAN_POINT ( 'NONE',  ( -19.64171699416042571, -5.764624264842452384, 11.49999999999999645 ) ) ;
#50155=EDGE_CURVE ( 'NONE', #30829, #80400, #14093, .T. ) ;
#50156=CARTESIAN_POINT ( 'NONE',  ( -118.6228709571500701, -24.65952944569305316, 1.056160979905706565 ) ) ;
#50157=VECTOR ( 'NONE', #63471, 1000.000000000000114 ) ;
#50160=CARTESIAN_POINT ( 'NONE',  ( -39.48699591144466581, -25.18431008553413974, 3.925287068261696266 ) ) ;
#50161=CARTESIAN_POINT ( 'NONE',  ( -60.62287095715004881, -29.50248789122583659, 2.256150453626215580 ) ) ;
#50162=LINE ( 'NONE', #33421, #32797 ) ;
#50163=EDGE_CURVE ( 'NONE', #64023, #32109, #44308, .T. ) ;
#50164=CARTESIAN_POINT ( 'NONE',  ( -109.6235285405774249, -24.65952944569305316, 1.056160979905708786 ) ) ;
#50167=CARTESIAN_POINT ( 'NONE',  ( 21.12055942831636202, -9.126644407798330860, 11.49999999999999645 ) ) ;
#50168=CARTESIAN_POINT ( 'NONE',  ( 21.64774270073068863, 7.000884456547583845, -1.500000000000002220 ) ) ;
#50169=CARTESIAN_POINT ( 'NONE',  ( -110.6263895210551595, -24.63419186844610920, 9.035850630976920428 ) ) ;
#50171=CARTESIAN_POINT ( 'NONE',  ( -90.55339685531903626, -24.15503026093913164, -0.2815557561904542538 ) ) ;
#50174=CARTESIAN_POINT ( 'NONE',  ( -18.37190169643047355, -11.86832528159398237, 11.49999999999998934 ) ) ;
#50175=CARTESIAN_POINT ( 'NONE',  ( -69.64019056953976872, -23.96169478059712787, 10.65365249895718414 ) ) ;
#50177=CARTESIAN_POINT ( 'NONE',  ( -51.04357394935764347, -25.31543073408252553, 4.940877929217665887 ) ) ;
#50178=CARTESIAN_POINT ( 'NONE',  ( -96.52287095715006160, -23.47596703998600631, 11.44779298504228215 ) ) ;
#50179=VERTEX_POINT ( 'NONE', #13827 ) ;
#50180=CARTESIAN_POINT ( 'NONE',  ( 9.511415417357532931, -18.05363124325620205, -1.500000000000002220 ) ) ;
#50181=ORIENTED_EDGE ( 'NONE', *, *, #50529, .T. ) ;
#50184=EDGE_LOOP ( 'NONE', ( #94516, #20790, #75786, #88977 ) ) ;
#50185=CARTESIAN_POINT ( 'NONE',  ( -18.14924840124409045, -14.16824886576183040, 11.49999999999998934 ) ) ;
#50186=DIRECTION ( 'NONE',  ( -0.000000000000000000, 2.173523156925979552E-06, -0.9999999999976378895 ) ) ;
#50187=CARTESIAN_POINT ( 'NONE',  ( 17.48260522047220888, -10.12088315688240314, -1.500000000000002220 ) ) ;
#50188=ORIENTED_EDGE ( 'NONE', *, *, #43400, .F. ) ;
#50191=CARTESIAN_POINT ( 'NONE',  ( -95.58514916329862388, -24.83618233451450408, 1.606449574219538157 ) ) ;
#50192=CARTESIAN_POINT ( 'NONE',  ( -53.56013297064492917, -23.73791477778911840, 11.05961554403170766 ) ) ;
#50193=CARTESIAN_POINT ( 'NONE',  ( -11.99125074976391048, 17.70416384622758343, 11.49999999999999645 ) ) ;
#50194=VERTEX_POINT ( 'NONE', #65664 ) ;
#50195=CARTESIAN_POINT ( 'NONE',  ( -79.22287095715006444, -23.47596703998600631, 11.44779298504227860 ) ) ;
#50196=EDGE_LOOP ( 'NONE', ( #77719, #80259, #62718, #34824 ) ) ;
#50197=CARTESIAN_POINT ( 'NONE',  ( -12.31279356157217109, -18.55646752483835016, -1.500000000000002220 ) ) ;
#50198=CARTESIAN_POINT ( 'NONE',  ( -18.22997975830956108, -9.740667652671243459, 11.49999999999998934 ) ) ;
#50200=ORIENTED_EDGE ( 'NONE', *, *, #98010, .F. ) ;
#50205=AXIS2_PLACEMENT_3D ( 'NONE', #92451, #5729, #61029 ) ;
#50208=CARTESIAN_POINT ( 'NONE',  ( -8.531171415479239073, -19.09552649099111221, -1.500000000000002220 ) ) ;
#50209=CARTESIAN_POINT ( 'NONE',  ( -21.90371867972833542, 1.011951690471867060, 11.49999999999999645 ) ) ;
#50210=CARTESIAN_POINT ( 'NONE',  ( -73.58434121117628024, -24.51419770103157347, 9.386484678747175181 ) ) ;
#50211=CARTESIAN_POINT ( 'NONE',  ( -14.39138815452349718, -17.32352244779961481, 11.49999999999998934 ) ) ;
#50213=CARTESIAN_POINT ( 'NONE',  ( 2.313481123293766206, -20.83243486019555135, -1.500000000000002220 ) ) ;
#50214=CARTESIAN_POINT ( 'NONE',  ( -38.58689981970802307, -24.34968618360933235, 0.1864209137778849723 ) ) ;
#50216=CARTESIAN_POINT ( 'NONE',  ( -119.5526336030634695, -24.66019654487200441, 8.947790411086108620 ) ) ;
#50220=VECTOR ( 'NONE', #88346, 1000.000000000000114 ) ;
#50222=CARTESIAN_POINT ( 'NONE',  ( -99.29890324015507019, -25.26221131662738628, 6.243173681414228682 ) ) ;
#50224=EDGE_CURVE ( 'NONE', #44267, #12270, #85645, .T. ) ;
#50226=CARTESIAN_POINT ( 'NONE',  ( 19.19993882694861753, 9.668096177433461946, -1.500000000000002220 ) ) ;
#50227=B_SPLINE_CURVE_WITH_KNOTS ( 'NONE', 3,
 ( #19538, #20044, #74333, #51007 ),
 .UNSPECIFIED., .F., .F.,
 ( 4, 4 ),
 ( 0.000000000000000000, 9.999999999994735322E-05 ),
 .UNSPECIFIED. ) ;
#50228=CARTESIAN_POINT ( 'NONE',  ( -59.52287095715006870, -23.73907113216987952, -1.053371485793253459 ) ) ;
#50229=CARTESIAN_POINT ( 'NONE',  ( 19.72786461798894209, 7.474574171381012100, 11.49999999999998934 ) ) ;
#50232=ADVANCED_FACE ( 'NONE', ( #22919 ), #46795, .T. ) ;
#50233=CARTESIAN_POINT ( 'NONE',  ( -87.62287095715008434, -23.96127896941631619, -0.6493128931037798202 ) ) ;
#50234=CARTESIAN_POINT ( 'NONE',  ( -99.12380231474227799, -29.50249168492682728, 4.001565943926128632 ) ) ;
#50235=CARTESIAN_POINT ( 'NONE',  ( -129.5897715217587063, -24.15620529776629510, 10.23563542870659759 ) ) ;
#50236=CARTESIAN_POINT ( 'NONE',  ( -16.84257673422482426, -14.26466048179180568, -1.500000000000002220 ) ) ;
#50237=EDGE_LOOP ( 'NONE', ( #66294, #86697, #60697, #28247 ) ) ;
#50238=CARTESIAN_POINT ( 'NONE',  ( -65.64503599903511599, -24.15602025860896518, 10.28564288303535257 ) ) ;
#50240=CARTESIAN_POINT ( 'NONE',  ( -41.56322468833811712, -25.27955966736181992, 5.062029455345571805 ) ) ;
#50242=EDGE_CURVE ( 'NONE', #64856, #30322, #44496, .T. ) ;
#50243=CARTESIAN_POINT ( 'NONE',  ( -25.50557291889858647, -24.91754783335685985, 3.798368663089755515 ) ) ;
#50244=EDGE_CURVE ( 'NONE', #11737, #19028, #100046, .T. ) ;
#50246=CARTESIAN_POINT ( 'NONE',  ( -6.767052838139933080, -20.26514109264706676, -1.500000000000002220 ) ) ;
#50247=CARTESIAN_POINT ( 'NONE',  ( -97.62287095715011276, -24.35013146730204170, 9.818937971375104823 ) ) ;
#50248=CARTESIAN_POINT ( 'NONE',  ( -90.70836042551606226, -25.31973986624387862, 5.294390042787146200 ) ) ;
#50249=CARTESIAN_POINT ( 'NONE',  ( -70.62287095715005592, -24.99156045073392463, 7.747789690856161648 ) ) ;
#50250=FACE_OUTER_BOUND ( 'NONE', #85604, .T. ) ;
#50251=CARTESIAN_POINT ( 'NONE',  ( 11.36372850657041589, -19.49111573544105624, -1.500000000000002220 ) ) ;
#50252=CARTESIAN_POINT ( 'NONE',  ( -65.58953762381672448, -24.99156044556120193, 7.747789690856343725 ) ) ;
#50253=ORIENTED_EDGE ( 'NONE', *, *, #12771, .F. ) ;
#50255=CARTESIAN_POINT ( 'NONE',  ( -42.52287095715005449, -29.50250243563736774, 8.947779886222148704 ) ) ;
#50256=CARTESIAN_POINT ( 'NONE',  ( -12.15653940608521566, -15.58205587995076868, 11.49999999999999645 ) ) ;
#50257=CARTESIAN_POINT ( 'NONE',  ( -59.62287095715007723, -23.96127896941632685, -0.6493128931037863705 ) ) ;
#50258=CARTESIAN_POINT ( 'NONE',  ( -67.50094105798223154, -24.34968618360932879, 0.1864209137778810865 ) ) ;
#50259=EDGE_CURVE ( 'NONE', #10252, #2274, #21452, .T. ) ;
#50261=CARTESIAN_POINT ( 'NONE',  ( -32.50560602629348494, -29.50248678627064081, 1.747779886239157809 ) ) ;
#50262=CARTESIAN_POINT ( 'NONE',  ( -70.52287095715007581, -23.48786465467241769, 11.44779295918254647 ) ) ;
#50263=DIRECTION ( 'NONE',  ( -3.773278334444166432E-23, 1.000000000000000000, 0.000000000000000000 ) ) ;
#50264=CARTESIAN_POINT ( 'NONE',  ( -17.57154585214776077, 12.61476001598989782, 11.49999999999998934 ) ) ;
#50266=CARTESIAN_POINT ( 'NONE',  ( -66.52287095715003318, -24.66019654487199375, 8.947790411086119278 ) ) ;
#50268=CARTESIAN_POINT ( 'NONE',  ( -41.62287095715006302, -29.50247984919015209, -1.443849546365060466 ) ) ;
#50269=CARTESIAN_POINT ( 'NONE',  ( -19.19514693104756375, 4.742496307885142315, -1.500000000000002220 ) ) ;
#50270=VERTEX_POINT ( 'NONE', #612 ) ;
#50271=CARTESIAN_POINT ( 'NONE',  ( -20.21730713243277933, 1.494317884549376974, 11.49999999999999645 ) ) ;
#50274=EDGE_CURVE ( 'NONE', #80473, #77786, #54910, .T. ) ;
#50275=ADVANCED_FACE ( 'NONE', ( #99057 ), #91957, .T. ) ;
#50277=CARTESIAN_POINT ( 'NONE',  ( -45.62287095715004881, -23.48783264082478084, -1.443836473390070374 ) ) ;
#50278=CARTESIAN_POINT ( 'NONE',  ( -106.9228709571500673, -23.47596703998600631, 11.44779298504227860 ) ) ;
#50283=CARTESIAN_POINT ( 'NONE',  ( 14.85562765054232059, -13.46834898924134372, 11.49999999999998934 ) ) ;
#50284=EDGE_CURVE ( 'NONE', #81499, #79071, #49175, .T. ) ;
#50286=ORIENTED_EDGE ( 'NONE', *, *, #28812, .F. ) ;
#50288=EDGE_CURVE ( 'NONE', #50993, #75137, #21930, .T. ) ;
#50289=VECTOR ( 'NONE', #8520, 1000.000000000000114 ) ;
#50290=CARTESIAN_POINT ( 'NONE',  ( -50.34997525821440689, -25.26258885166322088, 4.735128382460500163 ) ) ;
#50294=CARTESIAN_POINT ( 'NONE',  ( -95.62287095715005592, -29.50247984919015209, -1.443849546365050029 ) ) ;
#50295=CARTESIAN_POINT ( 'NONE',  ( -73.63908853846434965, -23.96119346886880663, -0.6495511937832115779 ) ) ;
#50296=VECTOR ( 'NONE', #68578, 1000.000000000000114 ) ;
#50298=AXIS2_PLACEMENT_3D ( 'NONE', #30314, #46061, #13586 ) ;
#50299=CARTESIAN_POINT ( 'NONE',  ( -51.54504057323880772, -25.12100811749006724, 7.112893600995336740 ) ) ;
#50300=ORIENTED_EDGE ( 'NONE', *, *, #19841, .F. ) ;
#50301=CARTESIAN_POINT ( 'NONE',  ( -0.6891947355827284794, 20.32259304938107292, 11.49999999999998934 ) ) ;
#50302=ORIENTED_EDGE ( 'NONE', *, *, #95655, .F. ) ;
#50303=CARTESIAN_POINT ( 'NONE',  ( -22.40196285382242536, -4.882868457752029379, -1.500000000000002220 ) ) ;
#50306=CARTESIAN_POINT ( 'NONE',  ( -109.5228709571501469, -24.34917612406837861, 0.1852690917426614847 ) ) ;
#50308=B_SPLINE_CURVE_WITH_KNOTS ( 'NONE', 3,
 ( #21334, #92357, #6124, #37076, #68041, #87250 ),
 .UNSPECIFIED., .F., .F.,
 ( 4, 2, 4 ),
 ( 1.570755371634454886E-05, 0.001396183895866091439, 0.002776660238015838614 ),
 .UNSPECIFIED. ) ;
#50310=CARTESIAN_POINT ( 'NONE',  ( -16.93204426113827310, 12.72334981527875186, 11.49999999999999645 ) ) ;
#50311=CARTESIAN_POINT ( 'NONE',  ( 12.08182546098005972, -18.57710416600862402, 11.49999999999998934 ) ) ;
#50312=CARTESIAN_POINT ( 'NONE',  ( 4.697267095454844998, -20.06606415395816967, -1.500000000000002220 ) ) ;
#50313=B_SPLINE_CURVE_WITH_KNOTS ( 'NONE', 3,
 ( #28082, #5730, #12342, #28572, #35694, #50925 ),
 .UNSPECIFIED., .F., .F.,
 ( 4, 2, 4 ),
 ( 6.391158118958419274E-06, 0.001387004593080773786, 0.002767618028042589419 ),
 .UNSPECIFIED. ) ;
#50315=CARTESIAN_POINT ( 'NONE',  ( -41.55303143007999722, -23.96119346886880663, -0.6495511937831991434 ) ) ;
#50316=ORIENTED_EDGE ( 'NONE', *, *, #29760, .T. ) ;
#50317=CARTESIAN_POINT ( 'NONE',  ( -54.54771575810656259, -24.15543982623906416, -0.2315651400026691176 ) ) ;
#50318=CARTESIAN_POINT ( 'NONE',  ( -126.6228709571500559, -23.48786465467242124, 11.44779295918253403 ) ) ;
#50319=ORIENTED_EDGE ( 'NONE', *, *, #32701, .F. ) ;
#50321=EDGE_LOOP ( 'NONE', ( #62687, #70663, #14901, #99100 ) ) ;
#50323=CARTESIAN_POINT ( 'NONE',  ( -28.49462909715936831, -23.99193123636717218, 10.23563545308467226 ) ) ;
#50325=CARTESIAN_POINT ( 'NONE',  ( 11.01739540223112357, 17.63107602209319680, -1.500000000000002220 ) ) ;
#50326=CARTESIAN_POINT ( 'NONE',  ( -19.66401359581072583, -9.230316601043258018, 11.49999999999999645 ) ) ;
#50327=VERTEX_POINT ( 'NONE', #37673 ) ;
#50330=CARTESIAN_POINT ( 'NONE',  ( 11.36419782745769069, 19.35538867594532775, 11.49999999999998934 ) ) ;
#50336=ORIENTED_EDGE ( 'NONE', *, *, #27550, .F. ) ;
#50338=AXIS2_PLACEMENT_3D ( 'NONE', #31599, #37716, #100086 ) ;
#50339=CARTESIAN_POINT ( 'NONE',  ( -69.62287095715005592, -24.66019654487199020, 8.947790411086131712 ) ) ;
#50340=ORIENTED_EDGE ( 'NONE', *, *, #21798, .F. ) ;
#50342=CARTESIAN_POINT ( 'NONE',  ( -14.93283513470682067, -15.21490397768744529, -1.500000000000002220 ) ) ;
#50343=ORIENTED_EDGE ( 'NONE', *, *, #84028, .T. ) ;
#50344=CARTESIAN_POINT ( 'NONE',  ( -88.52215625292510026, -23.48783264082476663, -1.443836473390093467 ) ) ;
#50345=EDGE_CURVE ( 'NONE', #52778, #37312, #90305, .T. ) ;
#50346=CARTESIAN_POINT ( 'NONE',  ( 4.919149715316761373, 21.27959583485438344, 11.49999999999998934 ) ) ;
#50347=PLANE ( 'NONE',  #7633 ) ;
#50348=CARTESIAN_POINT ( 'NONE',  ( 19.67839991682829748, -11.23141783594569354, -1.500000000000002220 ) ) ;
#50350=CARTESIAN_POINT ( 'NONE',  ( -49.52287095715004739, -24.66019654487198665, 8.947790411086131712 ) ) ;
#50351=CARTESIAN_POINT ( 'NONE',  ( -21.08706934527708654, 5.832127334627817739, -1.500000000000002220 ) ) ;
#50352=CARTESIAN_POINT ( 'NONE',  ( -66.62287095715008434, -23.96127896941632685, -0.6493128931037854823 ) ) ;
#50353=VERTEX_POINT ( 'NONE', #53413 ) ;
#50355=CARTESIAN_POINT ( 'NONE',  ( -126.5562042904833930, -24.65952944569305316, 1.056160979905706121 ) ) ;
#50356=EDGE_CURVE ( 'NONE', #35380, #69709, #81855, .T. ) ;
#50359=ADVANCED_FACE ( 'NONE', ( #49313 ), #30549, .T. ) ;
#50360=CARTESIAN_POINT ( 'NONE',  ( -90.62287095715002749, -24.52232992886364116, 0.6492154411906042588 ) ) ;
#50362=EDGE_LOOP ( 'NONE', ( #30083, #93860, #66894 ) ) ;
#50364=ADVANCED_FACE ( 'NONE', ( #56928 ), #17340, .T. ) ;
#50365=CARTESIAN_POINT ( 'NONE',  ( -20.42750280573200783, -23.78525073545353408, 0.8294870405985487194 ) ) ;
#50366=CARTESIAN_POINT ( 'NONE',  ( -19.37389216307569129, 8.798533688548827669, -1.500000000000002220 ) ) ;
#50369=DIRECTION ( 'NONE',  ( -3.773278334453080206E-23, 0.9999999999976377785, 2.173523156925979975E-06 ) ) ;
#50370=B_SPLINE_CURVE_WITH_KNOTS ( 'NONE', 3,
 ( #25979, #88890, #2659, #95993 ),
 .UNSPECIFIED., .F., .F.,
 ( 4, 4 ),
 ( 2.275056424024757261E-09, 0.0003976735161906177281 ),
 .UNSPECIFIED. ) ;
#50371=CARTESIAN_POINT ( 'NONE',  ( -68.54455071335534910, -24.34968618360933590, 0.1864209137778813363 ) ) ;
#50373=ORIENTED_EDGE ( 'NONE', *, *, #57296, .T. ) ;
#50374=CARTESIAN_POINT ( 'NONE',  ( -18.58057592369839384, -6.135153870360039896, 11.49999999999999645 ) ) ;
#50375=CARTESIAN_POINT ( 'NONE',  ( -108.5228709571500758, -23.72773821059537269, 11.05748984161097681 ) ) ;
#50376=CARTESIAN_POINT ( 'NONE',  ( -29.71696354036009780, -25.17832945473821837, 6.228946167112972887 ) ) ;
#50377=ADVANCED_FACE ( 'NONE', ( #10737 ), #63540, .F. ) ;
#50378=ORIENTED_EDGE ( 'NONE', *, *, #72131, .F. ) ;
#50379=CARTESIAN_POINT ( 'NONE',  ( -80.43221577628075636, -25.30553498687082481, 4.967019777649441359 ) ) ;
#50381=CARTESIAN_POINT ( 'NONE',  ( -52.52287095715006870, -29.50250786944525672, 11.44777988621624054 ) ) ;
#50382=DIRECTION ( 'NONE',  ( -3.773278334453079618E-23, 0.9999999999976377785, 2.173523156925979975E-06 ) ) ;
#50383=CARTESIAN_POINT ( 'NONE',  ( 16.89532177248590372, -10.13005384644002227, -1.500000000000002220 ) ) ;
#50384=EDGE_CURVE ( 'NONE', #5245, #16063, #44303, .T. ) ;
#50386=CARTESIAN_POINT ( 'NONE',  ( -78.52287095715004739, -23.48783264082476308, -1.443836473390091468 ) ) ;
#50388=ADVANCED_FACE ( 'NONE', ( #48302 ), #88361, .F. ) ;
#50390=ORIENTED_EDGE ( 'NONE', *, *, #76324, .F. ) ;
#50392=CARTESIAN_POINT ( 'NONE',  ( -60.22287095715005734, -23.47596703998600276, 11.44779298504227860 ) ) ;
#50393=CARTESIAN_POINT ( 'NONE',  ( -47.50673741778126669, -23.96119346886880663, -0.6495511937831951466 ) ) ;
#50394=CARTESIAN_POINT ( 'NONE',  ( -118.5537768141336556, -24.34968618360933945, 0.1864209137778906622 ) ) ;
#50395=CARTESIAN_POINT ( 'NONE',  ( -78.93018284415475705, -25.03722721891040948, 7.590183713343858329 ) ) ;
#50396=DIRECTION ( 'NONE',  ( -3.773278334453079618E-23, 0.9999999999976377785, 2.173523156925979975E-06 ) ) ;
#50397=CARTESIAN_POINT ( 'NONE',  ( -50.62287095715007013, -24.82558206586143257, 1.605769216559449708 ) ) ;
#50398=CARTESIAN_POINT ( 'NONE',  ( 1.593314845114734535, -19.89410510517485164, 11.49999999999998934 ) ) ;
#50399=CARTESIAN_POINT ( 'NONE',  ( -0.01140452636522266625, -22.90235944405398527, 6.868750951901480661 ) ) ;
#50400=CARTESIAN_POINT ( 'NONE',  ( 14.69432462292611952, 13.40460087117274490, -1.500000000000002220 ) ) ;
#50401=ORIENTED_EDGE ( 'NONE', *, *, #81833, .T. ) ;
#50403=EDGE_CURVE ( 'NONE', #78274, #23327, #21277, .T. ) ;
#50404=CARTESIAN_POINT ( 'NONE',  ( -29.52287095715006160, -24.26578402247989175, 9.819127079432160343 ) ) ;
#50406=CARTESIAN_POINT ( 'NONE',  ( 20.70993026999094511, 1.908435391604796028, 11.49999999999999645 ) ) ;
#50413=CARTESIAN_POINT ( 'NONE',  ( -127.5214699268525607, -24.15543982623907837, -0.2315651400026539075 ) ) ;
#50415=CARTESIAN_POINT ( 'NONE',  ( 19.68333694646799614, 4.735253856516091098, 11.49999999999998934 ) ) ;
#50417=CARTESIAN_POINT ( 'NONE',  ( -129.6228709571500417, -23.47593901973091235, -1.443836447538995760 ) ) ;
#50420=CARTESIAN_POINT ( 'NONE',  ( -79.34687923781922336, -25.27781941911278807, 5.960409260969139922 ) ) ;
#50423=CARTESIAN_POINT ( 'NONE',  ( 18.22975119132022215, -8.346483668847822557, -1.500000000000002220 ) ) ;
#50424=CARTESIAN_POINT ( 'NONE',  ( 20.40321384664088811, -4.974606123342796060, 11.49999999999999645 ) ) ;
#50426=CARTESIAN_POINT ( 'NONE',  ( -54.62287095715006302, -24.35013146730203815, 9.818937971375117257 ) ) ;
#50428=CARTESIAN_POINT ( 'NONE',  ( -9.261969182712835646, 20.05037652441878038, -1.500000000000002220 ) ) ;
#50429=CARTESIAN_POINT ( 'NONE',  ( -47.22287095715006444, -23.47593901973090169, -1.443836447538997980 ) ) ;
#50431=DIRECTION ( 'NONE',  ( 0.000000000000000000, -0.9999999999976377785, -2.173523156925979128E-06 ) ) ;
#50432=CARTESIAN_POINT ( 'NONE',  ( -72.51646567591126313, -23.73766607897670156, -1.055555164236458454 ) ) ;
#50433=CARTESIAN_POINT ( 'NONE',  ( -31.62287095715007013, -24.51283580621364067, 0.6167428607019773690 ) ) ;
#50436=CARTESIAN_POINT ( 'NONE',  ( -42.92287095715005307, -23.47596703998600276, 11.44779298504227683 ) ) ;
#50437=DIRECTION ( 'NONE',  ( 3.773278334444167608E-23, -1.000000000000000000, 0.000000000000000000 ) ) ;
#50438=PLANE ( 'NONE',  #89252 ) ;
#50439=CARTESIAN_POINT ( 'NONE',  ( 6.154377932377651739, 19.64630176443789367, -1.500000000000002220 ) ) ;
#50440=CARTESIAN_POINT ( 'NONE',  ( 8.794441374123232791, -19.68457759291379716, 11.49999999999999645 ) ) ;
#50441=ORIENTED_EDGE ( 'NONE', *, *, #43503, .T. ) ;
#50444=DIRECTION ( 'NONE',  ( 0.000000000000000000, 2.173523156925980399E-06, -0.9999999999976378895 ) ) ;
#50445=CARTESIAN_POINT ( 'NONE',  ( 11.81759748825469281, -18.92407201980706333, 11.49999999999998934 ) ) ;
#50447=DIRECTION ( 'NONE',  ( 3.773278334444166432E-23, -1.000000000000000000, 0.000000000000000000 ) ) ;
#50450=DIRECTION ( 'NONE',  ( -0.000000000000000000, 2.173523156925979552E-06, -0.9999999999976378895 ) ) ;
#50451=B_SPLINE_CURVE_WITH_KNOTS ( 'NONE', 3,
 ( #4257, #98579, #43812, #20956 ),
 .UNSPECIFIED., .F., .F.,
 ( 4, 4 ),
 ( 0.000000000000000000, 1.000000000000000000 ),
 .UNSPECIFIED. ) ;
#50452=CARTESIAN_POINT ( 'NONE',  ( 8.688630223215852766, -18.96179456382524364, -1.500000000000002220 ) ) ;
#50453=VERTEX_POINT ( 'NONE', #27955 ) ;
#50457=CARTESIAN_POINT ( 'NONE',  ( -50.60306404051401330, -25.30220920115066008, 4.715819228956954490 ) ) ;
#50458=CARTESIAN_POINT ( 'NONE',  ( 16.02493003730957000, -13.65669227992738577, -1.500000000000002220 ) ) ;
#50459=VERTEX_POINT ( 'NONE', #43193 ) ;
#50462=EDGE_CURVE ( 'NONE', #83385, #62297, #76986, .T. ) ;
#50463=DIRECTION ( 'NONE',  ( 0.000000000000000000, -0.9999999999976377785, -2.173523156925979128E-06 ) ) ;
#50464=EDGE_CURVE ( 'NONE', #74711, #46787, #12828, .T. ) ;
#50465=CARTESIAN_POINT ( 'NONE',  ( -76.50805816305593510, -24.15620529776628089, 10.23563542870660470 ) ) ;
#50466=DIRECTION ( 'NONE',  ( -3.773278334453079030E-23, 0.9999999999976377785, 2.173523156925979128E-06 ) ) ;
#50467=CARTESIAN_POINT ( 'NONE',  ( -4.559408409702599307, -21.23122434433648209, -1.500000000000002220 ) ) ;
#50468=CARTESIAN_POINT ( 'NONE',  ( -48.52287095715006160, -24.64965694238574656, 8.947790433994203596 ) ) ;
#50469=CARTESIAN_POINT ( 'NONE',  ( -13.35739915041183323, 17.77566839534079435, 11.49999999999999645 ) ) ;
#50471=CARTESIAN_POINT ( 'NONE',  ( -51.27521478229555640, -25.31441802849524692, 5.568540164726730524 ) ) ;
#50473=CARTESIAN_POINT ( 'NONE',  ( -36.58953762381672448, -23.48786465467240347, 11.44779295918255180 ) ) ;
#50475=ADVANCED_FACE ( 'NONE', ( #18838 ), #28950, .T. ) ;
#50476=ADVANCED_FACE ( 'NONE', ( #20322 ), #20825, .T. ) ;
#50477=CARTESIAN_POINT ( 'NONE',  ( -50.38191529551148307, -25.12049752546737835, 2.832404795212222659 ) ) ;
#50479=ORIENTED_EDGE ( 'NONE', *, *, #1684, .F. ) ;
#50481=VECTOR ( 'NONE', #60138, 1000.000000000000227 ) ;
#50482=DIRECTION ( 'NONE',  ( -3.773278334453079030E-23, 0.9999999999976377785, 2.173523156925979128E-06 ) ) ;
#50484=EDGE_CURVE ( 'NONE', #58811, #31528, #35859, .T. ) ;
#50487=CARTESIAN_POINT ( 'NONE',  ( -130.5728709571500872, -24.40567238644092640, 9.892971901584807881 ) ) ;
#50488=CARTESIAN_POINT ( 'NONE',  ( -21.13723655771239152, -7.639886366525781014, -1.500000000000002220 ) ) ;
#50490=CARTESIAN_POINT ( 'NONE',  ( -124.6228709571500559, -29.50248528299804818, 1.056150453629045360 ) ) ;
#50493=CARTESIAN_POINT ( 'NONE',  ( -116.5228709571500474, -24.50216790748204332, 0.6166512839542594993 ) ) ;
#50494=CARTESIAN_POINT ( 'NONE',  ( -30.59464630539410734, -24.75152770810919378, 1.363349870542269082 ) ) ;
#50495=CARTESIAN_POINT ( 'NONE',  ( 19.59400933563812330, 0.1774559437341752532, 11.49999999999998934 ) ) ;
#50496=CARTESIAN_POINT ( 'NONE',  ( -50.33461658617051171, -25.31263903432395779, 4.734677650700013452 ) ) ;
#50499=CARTESIAN_POINT ( 'NONE',  ( -10.32266838563235467, 18.89866041204108527, -1.500000000000002220 ) ) ;
#50501=CARTESIAN_POINT ( 'NONE',  ( -71.30218710724507503, -25.25639427085534905, 6.299238331127512858 ) ) ;
#50502=CARTESIAN_POINT ( 'NONE',  ( -50.52287095715006160, -24.91544648472626022, 1.928969306349430868 ) ) ;
#50503=CARTESIAN_POINT ( 'NONE',  ( -70.35895856474229504, -25.31161946917133321, 5.313173610579343453 ) ) ;
#50504=CARTESIAN_POINT ( 'NONE',  ( -19.49525799874905729, 12.17417675796824561, -1.500000000000002220 ) ) ;
#50507=CARTESIAN_POINT ( 'NONE',  ( -53.53688776224935708, -24.51314013834315730, 0.6176544820404108460 ) ) ;
#50508=CARTESIAN_POINT ( 'NONE',  ( 17.77915467781788195, 9.360003092772107181, 11.49999999999999645 ) ) ;
#50514=CARTESIAN_POINT ( 'NONE',  ( -9.893332137849947472, -17.22304987741864579, -1.500000000000002220 ) ) ;
#50515=CARTESIAN_POINT ( 'NONE',  ( -113.5165029720520238, -24.34968618360933945, 0.1864209137778880254 ) ) ;
#50516=CARTESIAN_POINT ( 'NONE',  ( 7.987771016649366729, -18.01272016045900415, -1.500000000000002220 ) ) ;
#50517=EDGE_CURVE ( 'NONE', #64861, #45470, #68560, .T. ) ;
#50518=CARTESIAN_POINT ( 'NONE',  ( -75.55620429048340725, -23.48786465467241058, 11.44779295918255180 ) ) ;
#50520=CARTESIAN_POINT ( 'NONE',  ( -115.6228709571500559, -23.47593901973091235, -1.443836447538997536 ) ) ;
#50521=CARTESIAN_POINT ( 'NONE',  ( -111.5228709571500616, -24.34917612406837151, 0.1852690917426604855 ) ) ;
#50522=CARTESIAN_POINT ( 'NONE',  ( 13.11803791274172681, -15.88952355948706341, 11.49999999999999645 ) ) ;
#50524=CARTESIAN_POINT ( 'NONE',  ( -121.5228709571500616, -24.65952944569305316, 1.056160979905705899 ) ) ;
#50525=B_SPLINE_CURVE_WITH_KNOTS ( 'NONE', 3,
 ( #56953, #87887, #11259, #88895 ),
 .UNSPECIFIED., .F., .F.,
 ( 4, 4 ),
 ( 0.000000000000000000, 9.999999999998897304E-05 ),
 .UNSPECIFIED. ) ;
#50526=CARTESIAN_POINT ( 'NONE',  ( -12.01393383709116947, -19.22582291892495121, 11.49999999999999645 ) ) ;
#50527=AXIS2_PLACEMENT_3D ( 'NONE', #82161, #82658, #36986 ) ;
#50528=ORIENTED_EDGE ( 'NONE', *, *, #87246, .F. ) ;
#50529=EDGE_CURVE ( 'NONE', #84514, #97228, #27418, .T. ) ;
#50530=CARTESIAN_POINT ( 'NONE',  ( -126.5895376238167245, -23.47593901973091235, -1.443836447538995760 ) ) ;
#50531=LINE ( 'NONE', #89094, #58198 ) ;
#50532=B_SPLINE_CURVE_WITH_KNOTS ( 'NONE', 3,
 ( #82688, #13169, #60870, #91795 ),
 .UNSPECIFIED., .F., .F.,
 ( 4, 4 ),
 ( 0.000000000000000000, 9.999999999997510880E-05 ),
 .UNSPECIFIED. ) ;
#50533=CARTESIAN_POINT ( 'NONE',  ( -111.9545715455114987, -25.05712135967895193, 7.447789548357302891 ) ) ;
#50534=PLANE ( 'NONE',  #65846 ) ;
#50537=LINE ( 'NONE', #27704, #76037 ) ;
#50538=CARTESIAN_POINT ( 'NONE',  ( -22.79553223295561892, 1.966428799096173075, 11.49999999999998934 ) ) ;
#50539=CARTESIAN_POINT ( 'NONE',  ( -91.62287095715004170, -29.50250243563736774, 8.947779886222139822 ) ) ;
#50540=CARTESIAN_POINT ( 'NONE',  ( -21.50746323947805649, 1.722430922125298247, -1.500000000000002220 ) ) ;
#50541=PLANE ( 'NONE',  #88471 ) ;
#50542=CARTESIAN_POINT ( 'NONE',  ( -65.52287095715006160, -24.52232992886361984, 0.6492154411906035927 ) ) ;
#50543=CARTESIAN_POINT ( 'NONE',  ( -6.869692127560369066, -21.44495933931894527, 11.49999999999999645 ) ) ;
#50546=B_SPLINE_CURVE_WITH_KNOTS ( 'NONE', 3,
 ( #85094, #45553, #93203, #76971 ),
 .UNSPECIFIED., .F., .F.,
 ( 4, 4 ),
 ( 0.000000000000000000, 9.999999999998897304E-05 ),
 .UNSPECIFIED. ) ;
#50548=CARTESIAN_POINT ( 'NONE',  ( 10.99670386783381737, -19.00842362925918749, 11.49999999999998934 ) ) ;
#50549=CARTESIAN_POINT ( 'NONE',  ( -111.6303161903200305, -23.73766607897671221, -1.055555164236450905 ) ) ;
#50551=ORIENTED_EDGE ( 'NONE', *, *, #79261, .F. ) ;
#50555=DIRECTION ( 'NONE',  ( 1.000000000000000000, 3.773278334444167608E-23, 8.201307833595939069E-29 ) ) ;
#50558=VERTEX_POINT ( 'NONE', #74621 ) ;
#50560=CARTESIAN_POINT ( 'NONE',  ( -110.2093792378191921, -29.50249512742697888, 5.585400078537770874 ) ) ;
#50561=CARTESIAN_POINT ( 'NONE',  ( -123.5228709571500616, -23.48786465467242479, 11.44779295918253759 ) ) ;
#50562=CARTESIAN_POINT ( 'NONE',  ( 18.17922461840205983, -9.147185827878928421, -1.500000000000002220 ) ) ;
#50565=CARTESIAN_POINT ( 'NONE',  ( -71.70484777582788638, -25.23825382336761081, 6.283456011705152555 ) ) ;
#50566=CARTESIAN_POINT ( 'NONE',  ( -38.52287095715006870, -29.50247984919015209, -1.443849546365060466 ) ) ;
#50568=B_SPLINE_CURVE_WITH_KNOTS ( 'NONE', 3,
 ( #97559, #35673, #51899, #27566, #60018, #36660 ),
 .UNSPECIFIED., .F., .F.,
 ( 4, 2, 4 ),
 ( 0.000000000000000000, 0.001380764517854763014, 0.002761529035709526028 ),
 .UNSPECIFIED. ) ;
#50569=AXIS2_PLACEMENT_3D ( 'NONE', #65489, #34014, #26400 ) ;
#50570=DIRECTION ( 'NONE',  ( -3.773278334453079030E-23, 0.9999999999976377785, 2.173523156925979128E-06 ) ) ;
#50571=CARTESIAN_POINT ( 'NONE',  ( -71.60924725748338915, -25.25855199099994053, 6.721927571088929021 ) ) ;
#50572=ORIENTED_EDGE ( 'NONE', *, *, #70513, .T. ) ;
#50573=CARTESIAN_POINT ( 'NONE',  ( -28.66129012810275256, -24.76880947087198237, 2.702369889720187324 ) ) ;
#50574=CARTESIAN_POINT ( 'NONE',  ( -97.55620429048339304, -24.66019654487200086, 8.947790411086128159 ) ) ;
#50577=CARTESIAN_POINT ( 'NONE',  ( -20.31193019649481357, 4.361987795224258946, -1.500000000000002220 ) ) ;
#50579=FACE_OUTER_BOUND ( 'NONE', #63214, .T. ) ;
#50582=FACE_OUTER_BOUND ( 'NONE', #23960, .T. ) ;
#50584=VERTEX_POINT ( 'NONE', #98448 ) ;
#50588=CARTESIAN_POINT ( 'NONE',  ( -86.52287095715009002, -24.33832256527048798, 0.1851278514138618714 ) ) ;
#50589=CARTESIAN_POINT ( 'NONE',  ( -43.51355794557933621, -23.73791477778911130, 11.05961554403171121 ) ) ;
#50590=CARTESIAN_POINT ( 'NONE',  ( -17.20036718215007099, 13.84871166177648583, 11.49999999999999645 ) ) ;
#50591=ORIENTED_EDGE ( 'NONE', *, *, #25289, .T. ) ;
#50592=CARTESIAN_POINT ( 'NONE',  ( -108.5121574744787267, -24.65952944569305316, 1.056160979905706121 ) ) ;
#50593=EDGE_CURVE ( 'NONE', #88484, #33442, #86707, .T. ) ;
#50594=CARTESIAN_POINT ( 'NONE',  ( -21.91535228782390732, -5.629186751109307885, 11.49999999999998934 ) ) ;
#50595=ADVANCED_FACE ( 'NONE', ( #30947 ), #45683, .F. ) ;
#50596=CARTESIAN_POINT ( 'NONE',  ( -115.5149135104634439, -24.73531770709096023, 8.716586749053508498 ) ) ;
#50599=ORIENTED_EDGE ( 'NONE', *, *, #99793, .T. ) ;
#50600=EDGE_CURVE ( 'NONE', #91623, #39871, #26144, .T. ) ;
#50602=VECTOR ( 'NONE', #16514, 1000.000000000000114 ) ;
#50603=CARTESIAN_POINT ( 'NONE',  ( -57.53785648602210046, -24.51419770103157703, 9.386484678747175181 ) ) ;
#50605=CARTESIAN_POINT ( 'NONE',  ( 7.804836024166685426, 19.70032748343534834, -1.500000000000002220 ) ) ;
#50607=CARTESIAN_POINT ( 'NONE',  ( -80.62287095715004170, -23.48786465467241058, 11.44779295918254469 ) ) ;
#50608=CARTESIAN_POINT ( 'NONE',  ( 18.98964132805693694, -11.70494588174365092, -1.500000000000002220 ) ) ;
#50611=ORIENTED_EDGE ( 'NONE', *, *, #33507, .T. ) ;
#50612=CARTESIAN_POINT ( 'NONE',  ( -125.5228709571500616, -29.50247984919015209, -1.443849546365044922 ) ) ;
#50613=FACE_OUTER_BOUND ( 'NONE', #38991, .T. ) ;
#50614=LINE ( 'NONE', #49629, #57718 ) ;
#50616=CARTESIAN_POINT ( 'NONE',  ( -16.16875682573952133, 10.94412424577950915, -1.500000000000002220 ) ) ;
#50618=CARTESIAN_POINT ( 'NONE',  ( -19.34459864454321831, 9.218434461607088792, 11.49999999999998934 ) ) ;
#50619=CARTESIAN_POINT ( 'NONE',  ( -26.72449842520168062, -24.57999555349612208, 1.897194066446994620 ) ) ;
#50623=CARTESIAN_POINT ( 'NONE',  ( -19.58686714514938387, 11.73587220785771379, -1.500000000000002220 ) ) ;
#50625=CARTESIAN_POINT ( 'NONE',  ( -102.5870889699518216, -24.51314013834316086, 0.6176544820404232805 ) ) ;
#50627=CARTESIAN_POINT ( 'NONE',  ( -1.345660788846553935, -19.86331345790170033, 11.49999999999999645 ) ) ;
#50628=CARTESIAN_POINT ( 'NONE',  ( -104.5551282687516448, -23.96119346886880663, -0.6495511937832033622 ) ) ;
#50629=CARTESIAN_POINT ( 'NONE',  ( -89.40841769935769889, -25.27880950044345809, 5.947789066509453271 ) ) ;
#50630=CARTESIAN_POINT ( 'NONE',  ( -48.65307323584794119, -23.73766607897670866, -1.055555164236436250 ) ) ;
#50632=FACE_OUTER_BOUND ( 'NONE', #25212, .T. ) ;
#50634=CARTESIAN_POINT ( 'NONE',  ( -32.40922458005066176, -25.16370864782812689, 7.203858152271859439 ) ) ;
#50635=CARTESIAN_POINT ( 'NONE',  ( 21.03555826204448209, -5.341079136732027166, 11.49999999999998934 ) ) ;
#50637=CARTESIAN_POINT ( 'NONE',  ( -15.85469643196389278, -11.46343829903102396, -1.500000000000002220 ) ) ;
#50638=CARTESIAN_POINT ( 'NONE',  ( -55.60865192297863757, -23.85049219812685806, 10.88485053497527133 ) ) ;
#50639=EDGE_CURVE ( 'NONE', #56586, #20842, #7911, .T. ) ;
#50641=B_SPLINE_CURVE_WITH_KNOTS ( 'NONE', 3,
 ( #83584, #74483, #6474, #45544, #61277, #5968, #99790, #37427 ),
 .UNSPECIFIED., .F., .F.,
 ( 4, 2, 2, 4 ),
 ( 6.384118678608731864E-06, 0.002007151183507255819, 0.003007534715921579473, 0.004007918248335902260 ),
 .UNSPECIFIED. ) ;
#50645=CARTESIAN_POINT ( 'NONE',  ( -19.95082702767638239, -4.354873812894156870, 11.49999999999999645 ) ) ;
#50646=CARTESIAN_POINT ( 'NONE',  ( -50.11049603129085739, -25.30358447871552841, 5.223373167154639063 ) ) ;
#50647=B_SPLINE_CURVE_WITH_KNOTS ( 'NONE', 3,
 ( #96305, #4954, #2973, #89691 ),
 .UNSPECIFIED., .F., .F.,
 ( 4, 4 ),
 ( 0.7310220049200362169, 0.7400284361921516396 ),
 .UNSPECIFIED. ) ;
#50648=FACE_OUTER_BOUND ( 'NONE', #82654, .T. ) ;
#50649=AXIS2_PLACEMENT_3D ( 'NONE', #70968, #40008, #84677 ) ;
#50651=EDGE_CURVE ( 'NONE', #16488, #3436, #98953, .T. ) ;
#50652=LINE ( 'NONE', #34925, #31364 ) ;
#50653=LINE ( 'NONE', #73485, #99521 ) ;
#50654=CARTESIAN_POINT ( 'NONE',  ( 2.021814659504407579E-13, -19.30000000000000426, -1.500000000000002220 ) ) ;
#50655=AXIS2_PLACEMENT_3D ( 'NONE', #40719, #17377, #9764 ) ;
#50656=ADVANCED_FACE ( 'NONE', ( #92342 ), #92123, .T. ) ;
#50657=CARTESIAN_POINT ( 'NONE',  ( -109.5138115999294968, -24.51314013834315375, 0.6176544820404177294 ) ) ;
#50659=DIRECTION ( 'NONE',  ( 1.000000000000000000, 3.773278334444166432E-23, 8.201307841325785021E-29 ) ) ;
#50660=CARTESIAN_POINT ( 'NONE',  ( 10.47623847176155820, -20.49086732513842080, 11.49999999999999645 ) ) ;
#50661=CARTESIAN_POINT ( 'NONE',  ( -17.61067154241388977, 14.45706175128816184, -1.500000000000002220 ) ) ;
#50662=CARTESIAN_POINT ( 'NONE',  ( -70.34543693012690824, -25.04307398257883577, 7.563174194274490780 ) ) ;
#50663=B_SPLINE_SURFACE_WITH_KNOTS ( 'NONE', 3, 1, ( 
 ( #44285, #5705 ),
 ( #75214, #7196 ),
 ( #69098, #30539 ),
 ( #53889, #8213 ),
 ( #24927, #71620 ),
 ( #93938, #47279 ),
 ( #17828, #39151 ),
 ( #86828, #70108 ),
 ( #16316, #79213 ),
 ( #31538, #71118 ),
 ( #77698, #2116 ),
 ( #79717, #64536 ),
 ( #23926, #40163 ),
 ( #62502, #33551 ),
 ( #10213, #93431 ) ),
 .UNSPECIFIED., .F., .F., .F.,
 ( 4, 1, 1, 1, 1, 1, 1, 1, 1, 1, 1, 1, 4 ),
 ( 2, 2 ),
 ( 0.000000000000000000, 0.09025424934267306520, 0.1785397915286855430, 0.2660930338538194384, 0.3546309779571704679, 0.4418861533505633599, 0.5257469151636473548, 0.6081136336036379042, 0.6901972728278812363, 0.7708214843303337060, 0.8483261812554098169, 0.9240117400247429558, 0.9999999999999998890 ),
 ( 0.000000000000000000, 1.000000000000000000 ),
 .UNSPECIFIED. ) ;
#50664=CARTESIAN_POINT ( 'NONE',  ( -40.52287095715009002, -24.91544648472626022, 1.928969306349431756 ) ) ;
#50665=FACE_OUTER_BOUND ( 'NONE', #98440, .T. ) ;
#50666=CARTESIAN_POINT ( 'NONE',  ( -54.52287095715004739, -23.96127896941631619, -0.6493128931038086860 ) ) ;
#50667=CARTESIAN_POINT ( 'NONE',  ( -89.52287095715010423, -24.34917612407033616, 0.1852690917477812227 ) ) ;
#50668=CARTESIAN_POINT ( 'NONE',  ( -21.73523922981167189, -2.474665994198115726, 11.49999999999998934 ) ) ;
#50670=CARTESIAN_POINT ( 'NONE',  ( -0.1426030150137701236, -21.20389190742571373, -1.497999999999532594 ) ) ;
#50671=AXIS2_PLACEMENT_3D ( 'NONE', #65, #91903, #85805 ) ;
#50673=CARTESIAN_POINT ( 'NONE',  ( -71.70647227915280553, -25.25299663069663936, 6.133628806981914927 ) ) ;
#50677=CARTESIAN_POINT ( 'NONE',  ( -12.60687543931603471, -16.05746371069360379, -1.500000000000002220 ) ) ;
#50678=VERTEX_POINT ( 'NONE', #32454 ) ;
#50682=CARTESIAN_POINT ( 'NONE',  ( -13.44081803467414638, 18.71018530922267686, 11.49999999999998934 ) ) ;
#50684=CARTESIAN_POINT ( 'NONE',  ( -6.497366621441947210, -19.08602653180391329, -1.500000000000002220 ) ) ;
#50685=VERTEX_POINT ( 'NONE', #3021 ) ;
#50686=FACE_OUTER_BOUND ( 'NONE', #96449, .T. ) ;
#50687=CARTESIAN_POINT ( 'NONE',  ( -91.62287095715004170, -29.50248528299804818, 1.056150453629040253 ) ) ;
#50688=CARTESIAN_POINT ( 'NONE',  ( -95.58939892478511524, -24.52300882791530512, 0.6510814631126408125 ) ) ;
#50689=CARTESIAN_POINT ( 'NONE',  ( -41.62287095715006302, -23.72773821059535493, 11.05748984161097503 ) ) ;
#50690=CARTESIAN_POINT ( 'NONE',  ( 8.370372042246325250, 19.68514866842044242, 11.49999999999999645 ) ) ;
#50695=CARTESIAN_POINT ( 'NONE',  ( 22.20168578472828358, 1.497490109320031682, -1.500000000000002220 ) ) ;
#50696=CARTESIAN_POINT ( 'NONE',  ( 20.35908867758196550, 3.722869731652943770, -1.500000000000002220 ) ) ;
#50699=VERTEX_POINT ( 'NONE', #39569 ) ;
#50700=CARTESIAN_POINT ( 'NONE',  ( -81.52287095715010423, -23.48783264083388289, -1.443836473375922580 ) ) ;
#50701=VERTEX_POINT ( 'NONE', #62928 ) ;
#50703=CARTESIAN_POINT ( 'NONE',  ( 0.7041596644206948863, -20.94928778062849162, -1.500000000000002220 ) ) ;
#50704=EDGE_CURVE ( 'NONE', #49734, #44058, #87715, .T. ) ;
#50705=CARTESIAN_POINT ( 'NONE',  ( -5.132426408838210108, -21.30661980433056968, 11.49999999999999645 ) ) ;
#50706=CARTESIAN_POINT ( 'NONE',  ( -26.38306202989770455, -24.89279797102699732, 6.654069566590164797 ) ) ;
#50707=CARTESIAN_POINT ( 'NONE',  ( 8.356338879324495039, -20.90460381316865934, -1.500000000000002220 ) ) ;
#50708=CARTESIAN_POINT ( 'NONE',  ( 20.71091302404612833, 3.140364381853995912, -1.500000000000002220 ) ) ;
#50709=CARTESIAN_POINT ( 'NONE',  ( -38.48005118028396510, -24.65952944569304606, 1.056160979905694131 ) ) ;
#50711=CARTESIAN_POINT ( 'NONE',  ( -119.5171998032949432, -24.66019654487200441, 8.947790411086108620 ) ) ;
#50713=CARTESIAN_POINT ( 'NONE',  ( -32.08503310962682065, -24.87219037988794312, 1.747789950295618899 ) ) ;
#50714=ORIENTED_EDGE ( 'NONE', *, *, #64488, .F. ) ;
#50717=ORIENTED_EDGE ( 'NONE', *, *, #39792, .T. ) ;
#50720=CARTESIAN_POINT ( 'NONE',  ( -52.57794712450625951, -24.65952944569304606, 1.056160979905696573 ) ) ;
#50721=EDGE_LOOP ( 'NONE', ( #71209, #55024, #8094, #1985 ) ) ;
#50722=CARTESIAN_POINT ( 'NONE',  ( 20.90071823198991297, 5.034746273075951351, -1.500000000000002220 ) ) ;
#50723=AXIS2_PLACEMENT_3D ( 'NONE', #15182, #84693, #46146 ) ;
#50724=CARTESIAN_POINT ( 'NONE',  ( -28.52287095715005805, -23.31185441368106126, 11.44779303854528685 ) ) ;
#50725=ORIENTED_EDGE ( 'NONE', *, *, #98497, .T. ) ;
#50726=CARTESIAN_POINT ( 'NONE',  ( -18.71117167593497399, 9.704403692310313190, -1.500000000000002220 ) ) ;
#50727=CARTESIAN_POINT ( 'NONE',  ( -92.58953762381672448, -24.64965694238407323, 8.947790433994651238 ) ) ;
#50728=CARTESIAN_POINT ( 'NONE',  ( -52.62287095715004881, -23.73907113216990439, -1.053371485793232143 ) ) ;
#50729=CARTESIAN_POINT ( 'NONE',  ( -50.54314373887315526, -24.40133493613049609, 9.663955038902804162 ) ) ;
#50730=CARTESIAN_POINT ( 'NONE',  ( -101.5853492316966822, -24.65952944569305316, 1.056160979905706121 ) ) ;
#50731=CARTESIAN_POINT ( 'NONE',  ( -109.3648162840242293, -25.29802075622466262, 4.345455213388392579 ) ) ;
#50732=CARTESIAN_POINT ( 'NONE',  ( -13.58966412916292299, 17.40808962483262690, -1.500000000000002220 ) ) ;
#50735=CARTESIAN_POINT ( 'NONE',  ( -116.5876151828773999, -24.65952944569305316, 1.056160979905712560 ) ) ;
#50736=EDGE_CURVE ( 'NONE', #65047, #66631, #39364, .T. ) ;
#50737=B_SPLINE_CURVE_WITH_KNOTS ( 'NONE', 3,
 ( #40650, #71600, #56387, #70086, #85302, #87309 ),
 .UNSPECIFIED., .F., .F.,
 ( 4, 2, 4 ),
 ( 0.000000000000000000, 0.001380901958385389412, 0.002761803916770778824 ),
 .UNSPECIFIED. ) ;
#50738=CARTESIAN_POINT ( 'NONE',  ( -108.9573313204422647, -25.28251216705303150, 4.249596787124276354 ) ) ;
#50739=CARTESIAN_POINT ( 'NONE',  ( -41.84702555354165554, -25.31624510665928796, 4.480638910303021305 ) ) ;
#50740=CARTESIAN_POINT ( 'NONE',  ( -62.53909850713881724, -24.51419770103156281, 9.386484678747184063 ) ) ;
#50741=FACE_OUTER_BOUND ( 'NONE', #33570, .T. ) ;
#50742=CARTESIAN_POINT ( 'NONE',  ( 21.34331307443176584, 0.5271963136488534429, 11.49999999999998934 ) ) ;
#50743=CARTESIAN_POINT ( 'NONE',  ( -26.12992370186784896, -24.95752881727359096, 5.611782011825503957 ) ) ;
#50744=FACE_OUTER_BOUND ( 'NONE', #19098, .T. ) ;
#50745=B_SPLINE_CURVE_WITH_KNOTS ( 'NONE', 3,
 ( #7710, #1109, #8723, #38152, #7203, #32051 ),
 .UNSPECIFIED., .F., .F.,
 ( 4, 2, 4 ),
 ( 0.000000000000000000, 0.001380764517854766050, 0.002761529035709532100 ),
 .UNSPECIFIED. ) ;
#50746=CARTESIAN_POINT ( 'NONE',  ( -84.58953762381672448, -24.66019654487199730, 8.947790411086112172 ) ) ;
#50747=FACE_OUTER_BOUND ( 'NONE', #48851, .T. ) ;
#50748=CARTESIAN_POINT ( 'NONE',  ( -17.75566480456612695, 14.03706703302619374, -1.500000000000002220 ) ) ;
#50749=B_SPLINE_SURFACE_WITH_KNOTS ( 'NONE', 3, 3, ( 
 ( #25040, #71231, #70227, #39266 ),
 ( #30663, #15924, #706, #93543 ),
 ( #62624, #24038, #54504, #84941 ),
 ( #17433, #1719, #23024, #78814 ),
 ( #32656, #48394, #47393, #61632 ),
 ( #77319, #46387, #63633, #85949 ),
 ( #63128, #9311, #62124, #56015 ) ),
 .UNSPECIFIED., .F., .F., .F.,
 ( 4, 3, 4 ),
 ( 4, 4 ),
 ( 0.0004766839783830419445, 0.1029713700210903166, 0.2054660560637975864 ),
 ( 0.009496412973245757505, 0.01051351915677940785 ),
 .UNSPECIFIED. ) ;
#50750=CARTESIAN_POINT ( 'NONE',  ( -65.52287095715006160, -24.99156044556202616, 7.747789690856173195 ) ) ;
#50752=CARTESIAN_POINT ( 'NONE',  ( -35.62287095715007013, -24.92604778743017491, 8.074972756849351896 ) ) ;
#50754=CARTESIAN_POINT ( 'NONE',  ( 10.86211995951333620, 16.47970581058804740, 11.49999999999999645 ) ) ;
#50756=CARTESIAN_POINT ( 'NONE',  ( -32.07722060962680644, -25.10952229683068282, 7.362941523434161084 ) ) ;
#50758=EDGE_LOOP ( 'NONE', ( #11410, #514, #32700, #44764 ) ) ;
#50760=CARTESIAN_POINT ( 'NONE',  ( -28.91304442625643034, -25.26026382785371283, 2.072903053319643529 ) ) ;
#50762=CARTESIAN_POINT ( 'NONE',  ( -101.1944152955115044, -25.17353290942304156, 6.858246026101943116 ) ) ;
#50763=CARTESIAN_POINT ( 'NONE',  ( -4.285004571687458963, -21.18589511591401831, -1.500000000000002220 ) ) ;
#50764=FACE_OUTER_BOUND ( 'NONE', #1042, .T. ) ;
#50765=CARTESIAN_POINT ( 'NONE',  ( -70.58953762381671027, -25.00158670708909270, 2.256160236439167299 ) ) ;
#50767=CARTESIAN_POINT ( 'NONE',  ( -80.68529634371549264, -25.04456290340675295, 7.556292259115348742 ) ) ;
#50768=CARTESIAN_POINT ( 'NONE',  ( -19.57314199983870751, -2.777824058246878280, -1.500000000000002220 ) ) ;
#50769=ADVANCED_FACE ( 'NONE', ( #93338 ), #9616, .F. ) ;
#50770=VERTEX_POINT ( 'NONE', #23830 ) ;
#50772=CARTESIAN_POINT ( 'NONE',  ( 18.82617747125253871, -7.458514806974097411, 11.49999999999999645 ) ) ;
#50773=CARTESIAN_POINT ( 'NONE',  ( -119.5228709571500474, -24.35013146730203815, 9.818937971375092388 ) ) ;
#50774=EDGE_CURVE ( 'NONE', #47959, #46913, #81781, .T. ) ;
#50775=EDGE_CURVE ( 'NONE', #51679, #34175, #1516, .T. ) ;
#50777=ORIENTED_EDGE ( 'NONE', *, *, #9109, .T. ) ;
#50778=CARTESIAN_POINT ( 'NONE',  ( -100.3686882637329063, -25.30212793431289953, 4.712266316240064867 ) ) ;
#50783=CARTESIAN_POINT ( 'NONE',  ( 17.67427751897593069, 9.450557017276361549, 11.49999999999998934 ) ) ;
#50787=CARTESIAN_POINT ( 'NONE',  ( -90.52287095715006160, -23.47596703998600631, 11.44779298504228393 ) ) ;
#50788=CARTESIAN_POINT ( 'NONE',  ( -104.6228709571500559, -29.50250243563736774, 8.947779886222138046 ) ) ;
#50792=EDGE_CURVE ( 'NONE', #91107, #94475, #33450, .T. ) ;
#50794=AXIS2_PLACEMENT_3D ( 'NONE', #46028, #94179, #38899 ) ;
#50795=FACE_OUTER_BOUND ( 'NONE', #45852, .T. ) ;
#50797=CARTESIAN_POINT ( 'NONE',  ( 0.8761431260907562857, 20.31601184897261092, 11.49999999999998934 ) ) ;
#50798=VECTOR ( 'NONE', #47361, 1000.000000000000114 ) ;
#50800=CARTESIAN_POINT ( 'NONE',  ( -20.69623851537618364, -9.862649113751288610, 11.49999999999998934 ) ) ;
#50802=EDGE_CURVE ( 'NONE', #59266, #23124, #25839, .T. ) ;
#50804=CARTESIAN_POINT ( 'NONE',  ( -37.62287095715005592, -23.47593901973091235, -1.443836447539011525 ) ) ;
#50805=EDGE_CURVE ( 'NONE', #12406, #91720, #16340, .T. ) ;
#50808=CARTESIAN_POINT ( 'NONE',  ( 15.74494995282791088, 14.18698661492608615, 11.49999999999999645 ) ) ;
#50809=CARTESIAN_POINT ( 'NONE',  ( -15.96568504569681402, -15.38390974582250692, -1.500000000000002220 ) ) ;
#50810=CARTESIAN_POINT ( 'NONE',  ( 20.46650637700042097, -2.330123182410055893, 11.49999999999998934 ) ) ;
#50811=EDGE_LOOP ( 'NONE', ( #17621, #93968, #30193, #46148 ) ) ;
#50812=CARTESIAN_POINT ( 'NONE',  ( -41.49888018455134642, -24.15543982623907127, -0.2315651400026566831 ) ) ;
#50815=DIRECTION ( 'NONE',  ( -1.000000000000000000, -3.773278334444166432E-23, -8.201307841325785021E-29 ) ) ;
#50817=ORIENTED_EDGE ( 'NONE', *, *, #60434, .T. ) ;
#50819=PLANE ( 'NONE',  #21062 ) ;
#50820=CARTESIAN_POINT ( 'NONE',  ( -28.52390393553966774, -24.49968521371325991, 8.947790409070464079 ) ) ;
#50822=CARTESIAN_POINT ( 'NONE',  ( -3.546427018491999483, -20.45703643143680850, -1.500000000000002220 ) ) ;
#50823=EDGE_CURVE ( 'NONE', #37127, #81082, #43078, .T. ) ;
#50824=CARTESIAN_POINT ( 'NONE',  ( 6.244050601037331560, 20.82503750550150912, 11.49999999999999645 ) ) ;
#50825=ORIENTED_EDGE ( 'NONE', *, *, #20226, .F. ) ;
#50828=CARTESIAN_POINT ( 'NONE',  ( -119.6228709571500701, -23.96177878511308634, 10.65340807706329507 ) ) ;
#50829=CARTESIAN_POINT ( 'NONE',  ( -14.39434090420295220, 17.20869321163716492, -1.500000000000002220 ) ) ;
#50830=CARTESIAN_POINT ( 'NONE',  ( -83.52287095715006160, -29.50248528299804818, 1.056150453629038477 ) ) ;
#50831=CARTESIAN_POINT ( 'NONE',  ( -0.1490770655183801252, -21.12008023607309681, -1.443836447538997758 ) ) ;
#50832=ORIENTED_EDGE ( 'NONE', *, *, #55091, .F. ) ;
#50834=CARTESIAN_POINT ( 'NONE',  ( -97.62287095715005592, -29.50248528299804818, 1.056150453629042030 ) ) ;
#50835=B_SPLINE_CURVE_WITH_KNOTS ( 'NONE', 3,
 ( #71971, #2452, #64375, #56755 ),
 .UNSPECIFIED., .F., .F.,
 ( 4, 4 ),
 ( 0.000000000000000000, 9.999999999999592548E-05 ),
 .UNSPECIFIED. ) ;
#50839=CARTESIAN_POINT ( 'NONE',  ( -46.53512403956532495, -24.51419770103157347, 9.386484678747180510 ) ) ;
#50840=ADVANCED_FACE ( 'NONE', ( #66923 ), #97842, .F. ) ;
#50842=CARTESIAN_POINT ( 'NONE',  ( -16.05942832139214360, -14.02155611864158402, -1.500000000000002220 ) ) ;
#50845=CARTESIAN_POINT ( 'NONE',  ( -88.51122574139041888, -24.15543982623907127, -0.2315651400026634277 ) ) ;
#50846=CARTESIAN_POINT ( 'NONE',  ( 16.32745387341675780, -14.53119815553504068, 11.49999999999998934 ) ) ;
#50848=CARTESIAN_POINT ( 'NONE',  ( -7.973561950239375307, 21.24132968703115765, 11.49999999999998934 ) ) ;
#50849=CARTESIAN_POINT ( 'NONE',  ( -41.42599659256448774, -25.18431008552816408, 3.925284320572509866 ) ) ;
#50851=CARTESIAN_POINT ( 'NONE',  ( 15.37660858059359725, 15.65766701038582021, -1.500000000000002220 ) ) ;
#50854=CARTESIAN_POINT ( 'NONE',  ( -122.5540027605393618, -24.51419770103158413, 9.386484678747169852 ) ) ;
#50855=LINE ( 'NONE', #4680, #29746 ) ;
#50856=EDGE_CURVE ( 'NONE', #95392, #47965, #98656, .T. ) ;
#50858=ORIENTED_EDGE ( 'NONE', *, *, #45751, .F. ) ;
#50859=CARTESIAN_POINT ( 'NONE',  ( -99.62287095715005592, -23.72773821059535848, 11.05748984161097503 ) ) ;
#50862=CARTESIAN_POINT ( 'NONE',  ( -20.41429444750324862, -24.04291568128049050, 1.633150109380534509 ) ) ;
#50863=CARTESIAN_POINT ( 'NONE',  ( -20.48789480994130230, 5.740754632170482097, -1.500000000000002220 ) ) ;
#50864=CARTESIAN_POINT ( 'NONE',  ( -98.54804105917907009, -24.51419770103155926, 9.386484678747176957 ) ) ;
#50865=CARTESIAN_POINT ( 'NONE',  ( -26.09929425038925999, -24.97064932688204664, 4.716438222426610594 ) ) ;
#50866=CARTESIAN_POINT ( 'NONE',  ( -85.53826683509211648, -25.00158670708911046, 2.256160236439219702 ) ) ;
#50867=CARTESIAN_POINT ( 'NONE',  ( -68.49381102065314053, -24.65952944569304606, 1.056160979905701236 ) ) ;
#50869=CARTESIAN_POINT ( 'NONE',  ( -117.5924224532624720, -23.73791477778912551, 11.05961554403169878 ) ) ;
#50871=CARTESIAN_POINT ( 'NONE',  ( 18.00893756148942870, 7.586210683597776949, 11.49999999999999645 ) ) ;
#50872=CARTESIAN_POINT ( 'NONE',  ( -67.52287095715006160, -24.66019654487199730, 8.947790411086115725 ) ) ;
#50874=B_SPLINE_CURVE_WITH_KNOTS ( 'NONE', 3,
 ( #55880, #23900, #62480, #63498 ),
 .UNSPECIFIED., .F., .F.,
 ( 4, 4 ),
 ( 0.000000000000000000, 9.999999999998897304E-05 ),
 .UNSPECIFIED. ) ;
#50875=CARTESIAN_POINT ( 'NONE',  ( -116.6228709571500417, -23.48786465467241769, 11.44779295918253759 ) ) ;
#50876=EDGE_LOOP ( 'NONE', ( #47820, #35334, #29023, #11512 ) ) ;
#50878=CARTESIAN_POINT ( 'NONE',  ( -101.1688285314437223, -25.06333783557038686, 7.418091300476992167 ) ) ;
#50879=B_SPLINE_CURVE_WITH_KNOTS ( 'NONE', 3,
 ( #91573, #39781, #76340, #70745, #8338, #6840, #37797, #68750, #69747, #77831, #32172, #54522, #99667, #30172, #15941, #8841 ),
 .UNSPECIFIED., .F., .F.,
 ( 4, 2, 2, 2, 2, 2, 2, 4 ),
 ( 0.000000000000000000, 0.0001833998957598680242, 0.0003667997915197360485, 0.0005501996872796041270, 0.0007335995830394720970, 0.001100399374559177029, 0.001283799270319020171, 0.001467199166078863096 ),
 .UNSPECIFIED. ) ;
#50881=CARTESIAN_POINT ( 'NONE',  ( -45.62287095715004881, -24.91544648472620338, 1.928969306349229473 ) ) ;
#50882=EDGE_CURVE ( 'NONE', #64842, #36479, #69558, .T. ) ;
#50883=CARTESIAN_POINT ( 'NONE',  ( 17.62393913918218402, -8.800128315780904487, 11.49999999999998934 ) ) ;
#50886=FACE_OUTER_BOUND ( 'NONE', #10011, .T. ) ;
#50890=CARTESIAN_POINT ( 'NONE',  ( -121.5228709571500616, -23.47596703998600631, 11.44779298504227860 ) ) ;
#50891=CARTESIAN_POINT ( 'NONE',  ( -104.9228709571501099, -23.47593901973090880, -1.443836447538997092 ) ) ;
#50892=CARTESIAN_POINT ( 'NONE',  ( -118.6235039205847386, -24.65952944569305316, 1.056160979905708119 ) ) ;
#50896=CARTESIAN_POINT ( 'NONE',  ( 19.80199147212610811, 2.383747631481649254, -1.500000000000002220 ) ) ;
#50898=CARTESIAN_POINT ( 'NONE',  ( -54.52287095715009002, -24.51387760970724372, 9.387446482453405849 ) ) ;
#50899=CARTESIAN_POINT ( 'NONE',  ( -0.05358151576393885979, -22.35634517190537807, 0.9392753064497983972 ) ) ;
#50900=ORIENTED_EDGE ( 'NONE', *, *, #82552, .T. ) ;
#50905=CARTESIAN_POINT ( 'NONE',  ( -122.6228709571500701, -23.48783264082479505, -1.443836473390058828 ) ) ;
#50907=CARTESIAN_POINT ( 'NONE',  ( -74.62287095715005592, -23.47593901973091235, -1.443836447539006196 ) ) ;
#50908=CARTESIAN_POINT ( 'NONE',  ( -50.66424699104888418, -25.18847548320762186, 3.319059850524417765 ) ) ;
#50913=VERTEX_POINT ( 'NONE', #89244 ) ;
#50914=CARTESIAN_POINT ( 'NONE',  ( 17.32893120472914816, 10.46255702124672027, 11.49999999999998934 ) ) ;
#50915=FACE_OUTER_BOUND ( 'NONE', #53109, .T. ) ;
#50916=B_SPLINE_CURVE_WITH_KNOTS ( 'NONE', 3,
 ( #37641, #70097, #30019, #61492, #16804, #69601, #577, #100011, #70595, #82, #8199, #91923, #39137, #46256 ),
 .UNSPECIFIED., .F., .F.,
 ( 4, 2, 2, 2, 2, 2, 4 ),
 ( 0.000000000000000000, 0.0001851154269384487790, 0.0003702308538768975580, 0.0007404617077537563015, 0.001110692561630614991, 0.001295807988569044064, 0.001480923415507472921 ),
 .UNSPECIFIED. ) ;
#50918=EDGE_CURVE ( 'NONE', #98447, #89470, #15093, .T. ) ;
#50919=ADVANCED_FACE ( 'NONE', ( #81128 ), #11609, .T. ) ;
#50922=ADVANCED_FACE ( 'NONE', ( #50686 ), #35463, .T. ) ;
#50925=CARTESIAN_POINT ( 'NONE',  ( -52.52287095715008292, -24.66019654487198665, 8.947790411086131712 ) ) ;
#50926=CARTESIAN_POINT ( 'NONE',  ( -2.827821146493835425, 19.88259668395040691, -1.500000000000002220 ) ) ;
#50927=CARTESIAN_POINT ( 'NONE',  ( -15.31302551872622075, -14.39686070098267479, 11.49999999999999645 ) ) ;
#50928=EDGE_CURVE ( 'NONE', #60977, #32935, #97355, .T. ) ;
#50929=CARTESIAN_POINT ( 'NONE',  ( -28.54571666164230948, -24.94250516244451532, 7.283072174430436974 ) ) ;
#50930=CARTESIAN_POINT ( 'NONE',  ( -89.81226385320381667, -25.26877915520014994, 5.947789088310639904 ) ) ;
#50931=CARTESIAN_POINT ( 'NONE',  ( -21.12782282263547984, 6.412464199276892707, -1.500000000000002220 ) ) ;
#50932=CARTESIAN_POINT ( 'NONE',  ( -42.52287095715005449, -24.64898659630367206, 1.056161002820819261 ) ) ;
#50933=CARTESIAN_POINT ( 'NONE',  ( -55.62287095715004170, -24.99132157543083821, 2.256160258750667502 ) ) ;
#50934=CARTESIAN_POINT ( 'NONE',  ( -50.10737344585005815, -25.27344765917630554, 3.323112495376625564 ) ) ;
#50936=CARTESIAN_POINT ( 'NONE',  ( -100.4381051993576364, -25.12049752546738191, 2.832404795212222215 ) ) ;
#50937=B_SPLINE_SURFACE_WITH_KNOTS ( 'NONE', 3, 3, ( 
 ( #93274, #55245, #86171, #94781 ),
 ( #32894, #54241, #15656, #63868 ),
 ( #63364, #70455, #23764, #53739 ),
 ( #77545, #62865, #16154, #38994 ),
 ( #17159, #94279, #61853, #47626 ),
 ( #54740, #433, #24762, #62349 ),
 ( #30886, #71463, #85674, #55745 ) ),
 .UNSPECIFIED., .F., .F., .F.,
 ( 4, 3, 4 ),
 ( 4, 4 ),
 ( 0.0004766839783822873398, 0.1029713700210899419, 0.2054660560637975864 ),
 ( 0.03950404640253154381, 0.04053499805299270314 ),
 .UNSPECIFIED. ) ;
#50940=ORIENTED_EDGE ( 'NONE', *, *, #55206, .T. ) ;
#50941=CARTESIAN_POINT ( 'NONE',  ( -55.52287095715005449, -25.00158670708909270, 2.256160236439166411 ) ) ;
#50943=CARTESIAN_POINT ( 'NONE',  ( -62.52287095715006160, -23.47593901973090169, -1.443836447538997092 ) ) ;
#50944=CARTESIAN_POINT ( 'NONE',  ( 9.149160795417088821, -18.46424698110740437, -1.500000000000002220 ) ) ;
#50946=CARTESIAN_POINT ( 'NONE',  ( -20.54356019850136050, 6.435454313062578535, 11.49999999999999645 ) ) ;
#50947=ORIENTED_EDGE ( 'NONE', *, *, #49409, .T. ) ;
#50948=CARTESIAN_POINT ( 'NONE',  ( -49.28469068309977530, -25.24826530213481846, 6.282384552296719882 ) ) ;
#50949=DIRECTION ( 'NONE',  ( -3.773278334453079618E-23, 0.9999999999976377785, 2.173523156925979975E-06 ) ) ;
#50951=CARTESIAN_POINT ( 'NONE',  ( 22.01400519847025450, -3.885951517071169370, 11.49999999999998934 ) ) ;
#50952=CARTESIAN_POINT ( 'NONE',  ( -59.62287095715004170, -24.35013146730203815, 9.818937971375111928 ) ) ;
#50954=EDGE_CURVE ( 'NONE', #76857, #7414, #84103, .T. ) ;
#50957=CARTESIAN_POINT ( 'NONE',  ( -51.70072539166533687, -25.26311289191998455, 3.987152081390995306 ) ) ;
#50958=B_SPLINE_CURVE_WITH_KNOTS ( 'NONE', 3,
 ( #92555, #15928, #46895, #8325, #17436, #3240, #88459, #16935, #2231, #34173, #57522, #95066, #48398, #25043 ),
 .UNSPECIFIED., .F., .F.,
 ( 4, 2, 2, 2, 2, 2, 4 ),
 ( 0.000000000000000000, 0.0003092239551898974103, 0.0004638359327848582585, 0.0006184479103798191067, 0.0009276718655697721366, 0.001082283843164748380, 0.001236895820759724733 ),
 .UNSPECIFIED. ) ;
#50959=CARTESIAN_POINT ( 'NONE',  ( 8.468106961216914641, 19.09613275528424836, -1.500000000000002220 ) ) ;
#50961=VECTOR ( 'NONE', #19309, 1000.000000000000114 ) ;
#50963=EDGE_CURVE ( 'NONE', #84227, #13356, #58781, .T. ) ;
#50964=ORIENTED_EDGE ( 'NONE', *, *, #96079, .T. ) ;
#50965=VERTEX_POINT ( 'NONE', #95853 ) ;
#50966=CARTESIAN_POINT ( 'NONE',  ( -100.6334151984021759, -24.15602025860896518, 10.28564288303536856 ) ) ;
#50967=CARTESIAN_POINT ( 'NONE',  ( -18.40674794014382698, -10.35651468716735657, -1.500000000000002220 ) ) ;
#50968=ORIENTED_EDGE ( 'NONE', *, *, #5798, .F. ) ;
#50969=CARTESIAN_POINT ( 'NONE',  ( -85.62287095715002749, -25.00182538069145011, 7.747789668545099317 ) ) ;
#50974=CARTESIAN_POINT ( 'NONE',  ( -20.31635052000798325, -7.690577546848336610, -1.500000000000002220 ) ) ;
#50975=CARTESIAN_POINT ( 'NONE',  ( -81.04964064216432007, -25.12224358380520783, 6.946763632574976199 ) ) ;
#50976=CARTESIAN_POINT ( 'NONE',  ( -11.95080204275630464, 18.75100984808165094, 11.49999999999999645 ) ) ;
#50977=EDGE_LOOP ( 'NONE', ( #54084, #27954, #94616, #38428 ) ) ;
#50978=FACE_OUTER_BOUND ( 'NONE', #33107, .T. ) ;
#50984=EDGE_CURVE ( 'NONE', #6550, #39939, #61120, .T. ) ;
#50985=CARTESIAN_POINT ( 'NONE',  ( -40.62287095715004170, -25.00158670708908204, 2.256160236439166411 ) ) ;
#50986=VERTEX_POINT ( 'NONE', #30837 ) ;
#50987=ORIENTED_EDGE ( 'NONE', *, *, #16004, .F. ) ;
#50988=CARTESIAN_POINT ( 'NONE',  ( -101.1944152955115186, -25.17323144036708626, 6.858246026757193192 ) ) ;
#50990=FACE_OUTER_BOUND ( 'NONE', #53224, .T. ) ;
#50991=CARTESIAN_POINT ( 'NONE',  ( -37.62287095715005592, -24.66019654487199020, 8.947790411086135265 ) ) ;
#50992=CARTESIAN_POINT ( 'NONE',  ( -66.52287095715010423, -23.72773821059536914, 11.05748984161097326 ) ) ;
#50993=VERTEX_POINT ( 'NONE', #29335 ) ;
#50994=CARTESIAN_POINT ( 'NONE',  ( -13.43510958081001050, -13.94331287200543024, 11.49999999999999645 ) ) ;
#50995=CARTESIAN_POINT ( 'NONE',  ( -69.52287095715006160, -23.47593901973090169, -1.443836447538996870 ) ) ;
#50996=CARTESIAN_POINT ( 'NONE',  ( -17.93832129671990572, 13.47109510200611560, -1.500000000000002220 ) ) ;
#50997=ORIENTED_EDGE ( 'NONE', *, *, #78839, .T. ) ;
#50999=DIRECTION ( 'NONE',  ( -3.773278334453079030E-23, 0.9999999999976377785, 2.173523156925979128E-06 ) ) ;
#51001=CARTESIAN_POINT ( 'NONE',  ( -63.92776651206412453, -24.47917135695840685, 9.440663514584127114 ) ) ;
#51002=CARTESIAN_POINT ( 'NONE',  ( 16.73968668634701729, 10.17700309559984717, -1.500000000000002220 ) ) ;
#51003=CARTESIAN_POINT ( 'NONE',  ( -46.48849370679067761, -24.51314013834315020, 0.6176544820404062941 ) ) ;
#51004=VERTEX_POINT ( 'NONE', #61802 ) ;
#51006=CARTESIAN_POINT ( 'NONE',  ( -20.49900048275977227, -6.559984590058941301, 11.49999999999998934 ) ) ;
#51007=CARTESIAN_POINT ( 'NONE',  ( -121.5228709571501042, -23.48783264082477018, -1.443836473390083253 ) ) ;
#51008=CARTESIAN_POINT ( 'NONE',  ( -71.28784841027113828, -25.25639446183122772, 6.387102990573659156 ) ) ;
#51009=DIRECTION ( 'NONE',  ( -3.773278334453080206E-23, 0.9999999999976377785, 2.173523156925979975E-06 ) ) ;
#51010=CARTESIAN_POINT ( 'NONE',  ( -99.52818128268205555, -25.27473369906244471, 3.976272290400146847 ) ) ;
#51011=CARTESIAN_POINT ( 'NONE',  ( 8.986065527603487979, -21.13286776747340667, -1.500000000000002220 ) ) ;
#51013=CARTESIAN_POINT ( 'NONE',  ( -61.62287095715004881, -29.50250243563736774, 8.947779886222145151 ) ) ;
#51015=CARTESIAN_POINT ( 'NONE',  ( -15.35229381799144299, -13.07563953244551591, 11.49999999999999645 ) ) ;
#51016=CARTESIAN_POINT ( 'NONE',  ( -109.1001591083545179, -25.28814224509513053, 3.548368719171229646 ) ) ;
#51017=CARTESIAN_POINT ( 'NONE',  ( -32.62373933420111882, -24.66019654487198665, 8.947790411086131712 ) ) ;
#51018=DIRECTION ( 'NONE',  ( -3.773278334444167608E-23, 1.000000000000000000, 0.000000000000000000 ) ) ;
#51020=CARTESIAN_POINT ( 'NONE',  ( -82.52287095715004739, -23.95044443724992789, 10.65354141964649592 ) ) ;
#51021=CARTESIAN_POINT ( 'NONE',  ( -12.84220538718065185, 15.17226672225704398, -1.500000000000002220 ) ) ;
#51023=CARTESIAN_POINT ( 'NONE',  ( 14.14096853472169535, -13.71769858867784464, -1.500000000000002220 ) ) ;
#51024=CARTESIAN_POINT ( 'NONE',  ( -42.63429243087625764, -24.34968618360933590, 0.1864209137778841396 ) ) ;
#51027=CARTESIAN_POINT ( 'NONE',  ( -9.157874670058189892, -18.46812626297970539, 11.49999999999999645 ) ) ;
#51028=CARTESIAN_POINT ( 'NONE',  ( -39.31539998891226162, -25.31628649467095116, 5.139621149922747989 ) ) ;
#51031=FACE_OUTER_BOUND ( 'NONE', #81297, .T. ) ;
#51032=CARTESIAN_POINT ( 'NONE',  ( -19.66899025692886838, 11.29834648773183581, 11.49999999999999645 ) ) ;
#51034=CARTESIAN_POINT ( 'NONE',  ( -86.52287095715001897, -23.73907113217710929, -1.053371485780543848 ) ) ;
#51036=EDGE_CURVE ( 'NONE', #23353, #51831, #49096, .T. ) ;
#51037=EDGE_CURVE ( 'NONE', #60506, #89004, #3085, .T. ) ;
#51039=VECTOR ( 'NONE', #40594, 1000.000000000000114 ) ;
#51040=ADVANCED_FACE ( 'NONE', ( #98337 ), #38661, .T. ) ;
#51041=CARTESIAN_POINT ( 'NONE',  ( -56.52287095715006870, -24.51387760970724372, 9.387446482453409402 ) ) ;
#51043=ORIENTED_EDGE ( 'NONE', *, *, #40871, .F. ) ;
#51046=CARTESIAN_POINT ( 'NONE',  ( -99.33852787251029781, -25.22239172282626285, 6.423926351378344890 ) ) ;
#51047=CARTESIAN_POINT ( 'NONE',  ( -9.520747347383798243, -20.79447232172871907, -1.500000000000002220 ) ) ;
#51048=CARTESIAN_POINT ( 'NONE',  ( -52.62287095715005592, -29.50250243563736774, 8.947779886222146928 ) ) ;
#51049=CARTESIAN_POINT ( 'NONE',  ( 14.26105141482337935, -16.23293960606763520, -1.500000000000002220 ) ) ;
#51050=CARTESIAN_POINT ( 'NONE',  ( -113.5154120510410536, -24.51419770103157347, 9.386484678747168076 ) ) ;
#51051=CARTESIAN_POINT ( 'NONE',  ( -115.5228709571500616, -24.99156044556202616, 7.747789690856173195 ) ) ;
#51052=CARTESIAN_POINT ( 'NONE',  ( 20.50669422456317292, -9.396423750077818937, 11.49999999999999645 ) ) ;
#51053=ORIENTED_EDGE ( 'NONE', *, *, #37873, .F. ) ;
#51054=CARTESIAN_POINT ( 'NONE',  ( -68.62287095715005592, -24.64965695001468404, 8.947790433994184056 ) ) ;
#51055=CARTESIAN_POINT ( 'NONE',  ( 21.11370014442628218, -6.196533921283487345, -1.500000000000002220 ) ) ;
#51056=CARTESIAN_POINT ( 'NONE',  ( -64.52287095715006160, -24.64898659630528854, 1.056161002820822592 ) ) ;
#51057=CARTESIAN_POINT ( 'NONE',  ( -112.5895376238167387, -24.64965694238407679, 8.947790433994649462 ) ) ;
#51058=EDGE_LOOP ( 'NONE', ( #64312, #64290, #68206, #30616 ) ) ;
#51059=LINE ( 'NONE', #89119, #86454 ) ;
#51061=ORIENTED_EDGE ( 'NONE', *, *, #9781, .T. ) ;
#51062=CARTESIAN_POINT ( 'NONE',  ( -76.52287095715007581, -29.50250243563736774, 8.947779886222141599 ) ) ;
#51064=ORIENTED_EDGE ( 'NONE', *, *, #33291, .F. ) ;
#51067=CARTESIAN_POINT ( 'NONE',  ( -100.4381051993576506, -25.11033443737754212, 2.832404817301930056 ) ) ;
#51069=CARTESIAN_POINT ( 'NONE',  ( 19.80222353126469415, -4.898785079568316547, -1.500000000000002220 ) ) ;
#51070=EDGE_LOOP ( 'NONE', ( #62192, #76174, #50343, #49764 ) ) ;
#51072=CARTESIAN_POINT ( 'NONE',  ( -51.01463207101524944, -25.14354145956054509, 2.962925292413864486 ) ) ;
#51073=CARTESIAN_POINT ( 'NONE',  ( -97.52287095715007581, -23.47593901973090524, -1.443836447538996648 ) ) ;
#51074=CARTESIAN_POINT ( 'NONE',  ( -71.70128661679227378, -25.25855123413748871, 6.373708393512837134 ) ) ;
#51075=ADVANCED_FACE ( 'NONE', ( #25220 ), #71918, .T. ) ;
#51078=CARTESIAN_POINT ( 'NONE',  ( -94.52287095715007581, -23.47593901973090524, -1.443836447538996648 ) ) ;
#51079=AXIS2_PLACEMENT_3D ( 'NONE', #85317, #93936, #76692 ) ;
#51081=CARTESIAN_POINT ( 'NONE',  ( -3.546427018491999483, -20.45703643143680850, -1.500000000000002220 ) ) ;
#51084=ORIENTED_EDGE ( 'NONE', *, *, #89843, .T. ) ;
#51085=DIRECTION ( 'NONE',  ( -3.773278334453079618E-23, 0.9999999999976377785, 2.173523156925979975E-06 ) ) ;
#51086=CARTESIAN_POINT ( 'NONE',  ( -129.5556839989185960, -24.66019654487200086, 8.947790411086113949 ) ) ;
#51087=EDGE_LOOP ( 'NONE', ( #9082, #31836, #1610, #26223 ) ) ;
#51090=CARTESIAN_POINT ( 'NONE',  ( -117.2170248000532951, -25.23482019547913424, 3.690485340690507154 ) ) ;
#51092=CARTESIAN_POINT ( 'NONE',  ( -43.54650061354490020, -24.15620529776627734, 10.23563542870661003 ) ) ;
#51093=CARTESIAN_POINT ( 'NONE',  ( 17.21905055353458991, -13.78536315820828229, 11.49999999999999645 ) ) ;
#51095=CARTESIAN_POINT ( 'NONE',  ( -119.6228709571500559, -29.50247984919015209, -1.443849546365046699 ) ) ;
#51096=CARTESIAN_POINT ( 'NONE',  ( -17.13258802378025791, -14.77425600068537115, -1.500000000000002220 ) ) ;
#51097=ADVANCED_FACE ( 'NONE', ( #7997 ), #17109, .T. ) ;
#51098=CARTESIAN_POINT ( 'NONE',  ( -115.5522222404271560, -24.63419186844613051, 9.035850630976920428 ) ) ;
#51099=ORIENTED_EDGE ( 'NONE', *, *, #88271, .F. ) ;
#51103=AXIS2_PLACEMENT_3D ( 'NONE', #29318, #60290, #91213 ) ;
#51104=CARTESIAN_POINT ( 'NONE',  ( -57.63796015616722457, -24.15620529776628089, 10.23563542870660470 ) ) ;
#51105=ORIENTED_EDGE ( 'NONE', *, *, #487, .F. ) ;
#51106=CARTESIAN_POINT ( 'NONE',  ( -20.37118330240554087, -5.769015352940915164, 11.49999999999998934 ) ) ;
#51107=CARTESIAN_POINT ( 'NONE',  ( -89.52287095715004739, -24.51387760970726148, 9.387446482453416507 ) ) ;
#51108=CARTESIAN_POINT ( 'NONE',  ( 10.43072250204971851, -19.66636941823637841, -1.500000000000002220 ) ) ;
#51110=VECTOR ( 'NONE', #78763, 1000.000000000000114 ) ;
#51112=CARTESIAN_POINT ( 'NONE',  ( -0.1426030150137709562, -21.20389190742572083, 11.50200000000000422 ) ) ;
#51113=CARTESIAN_POINT ( 'NONE',  ( -37.58096006492539942, -24.51314013834315375, 0.6176544820404124003 ) ) ;
#51115=CARTESIAN_POINT ( 'NONE',  ( -79.62287095715004170, -23.47596703998600631, 11.44779298504227860 ) ) ;
#51117=CARTESIAN_POINT ( 'NONE',  ( 16.96702763494397104, -9.608290155750392358, -1.500000000000002220 ) ) ;
#51118=CARTESIAN_POINT ( 'NONE',  ( 5.397486108853063236, 20.74927772461418485, -1.500000000000002220 ) ) ;
#51119=CARTESIAN_POINT ( 'NONE',  ( -26.85447117215736412, -24.92774709175325043, 1.825771349380765907 ) ) ;
#51121=CARTESIAN_POINT ( 'NONE',  ( -34.52287095715005449, -23.72747288104469732, -1.053458166803228346 ) ) ;
#51122=CARTESIAN_POINT ( 'NONE',  ( 4.306090731860143350, 22.38281141545218844, -1.500000000000002220 ) ) ;
#51124=CARTESIAN_POINT ( 'NONE',  ( -79.52287095715010423, -23.47593901973090524, -1.443836447538996870 ) ) ;
#51125=DIRECTION ( 'NONE',  ( -3.773278334453079030E-23, 0.9999999999976377785, 2.173523156925979128E-06 ) ) ;
#51126=CARTESIAN_POINT ( 'NONE',  ( 12.47747183659840786, 15.48776231947736015, 11.49999999999999645 ) ) ;
#51128=CARTESIAN_POINT ( 'NONE',  ( -71.52287095715007581, -24.64965694238408034, 8.947790433994200043 ) ) ;
#51133=CARTESIAN_POINT ( 'NONE',  ( 5.343276940429747768, -21.04383479052346217, -1.500000000000002220 ) ) ;
#51134=CARTESIAN_POINT ( 'NONE',  ( -94.52287095715006160, -24.64898659630367916, 1.056161002820827921 ) ) ;
#51135=CARTESIAN_POINT ( 'NONE',  ( 17.37147561666312257, 8.948746033654231269, -1.500000000000002220 ) ) ;
#51136=LINE ( 'NONE', #20673, #8566 ) ;
#51137=ORIENTED_EDGE ( 'NONE', *, *, #1952, .F. ) ;
#51139=VECTOR ( 'NONE', #81355, 1000.000000000000114 ) ;
#51141=CARTESIAN_POINT ( 'NONE',  ( -60.62287095715007723, -24.52323809116982645, 9.355190652339427260 ) ) ;
#51142=CARTESIAN_POINT ( 'NONE',  ( 16.92567061652012228, 11.46397006495115534, 11.49999999999999645 ) ) ;
#51144=CARTESIAN_POINT ( 'NONE',  ( -39.62287095715004881, -24.50321055353805022, 9.387540953477534700 ) ) ;
#51146=CARTESIAN_POINT ( 'NONE',  ( -62.62287095715009144, -23.96127896941632685, -0.6493128931037860374 ) ) ;
#51147=CARTESIAN_POINT ( 'NONE',  ( -106.6228709571500275, -24.33927499327855060, 9.819080762295810061 ) ) ;
#51151=CARTESIAN_POINT ( 'NONE',  ( -63.52287095715006160, -23.47596703998600631, 11.44779298504228926 ) ) ;
#51152=ADVANCED_FACE ( 'NONE', ( #62302 ), #48075, .T. ) ;
#51156=CARTESIAN_POINT ( 'NONE',  ( -14.90462150274475306, 17.49973755783957685, 11.49999999999999645 ) ) ;
#51157=CARTESIAN_POINT ( 'NONE',  ( -22.19569011343799048, 5.130922947863589378, 11.49999999999998934 ) ) ;
#51158=CARTESIAN_POINT ( 'NONE',  ( -70.35039385224574460, -25.30458797330573972, 4.853613872476585378 ) ) ;
#51160=CARTESIAN_POINT ( 'NONE',  ( -93.62287095715005592, -23.47593901973091235, -1.443836447539002865 ) ) ;
#51162=CARTESIAN_POINT ( 'NONE',  ( -50.55620429048339304, -25.00158670708909270, 2.256160236439166855 ) ) ;
#51164=CARTESIAN_POINT ( 'NONE',  ( -110.5132613601996070, -24.63355581998384380, 0.9682620441943931011 ) ) ;
#51165=CARTESIAN_POINT ( 'NONE',  ( 17.35060923807083810, -13.37414737355047656, 11.49999999999998934 ) ) ;
#51166=CARTESIAN_POINT ( 'NONE',  ( -59.62287095715004881, -24.64965695001468404, 8.947790433994185832 ) ) ;
#51167=VECTOR ( 'NONE', #72036, 1000.000000000000227 ) ;
#51168=DIRECTION ( 'NONE',  ( -3.773278334453079618E-23, 0.9999999999976377785, 2.173523156925979552E-06 ) ) ;
#51171=VERTEX_POINT ( 'NONE', #8998 ) ;
#51173=CARTESIAN_POINT ( 'NONE',  ( 1.124825640313904973, 20.40429917142216354, -1.500000000000002220 ) ) ;
#51175=VECTOR ( 'NONE', #52242, 1000.000000000000114 ) ;
#51177=ORIENTED_EDGE ( 'NONE', *, *, #40417, .T. ) ;
#51179=EDGE_CURVE ( 'NONE', #1598, #7141, #16106, .T. ) ;
#51180=CARTESIAN_POINT ( 'NONE',  ( 8.428894486204411507, 21.44871590506140890, -1.500000000000002220 ) ) ;
#51182=CARTESIAN_POINT ( 'NONE',  ( -13.58233929615340152, 14.99024694321910900, -1.500000000000002220 ) ) ;
#51185=CARTESIAN_POINT ( 'NONE',  ( -97.62287095715002749, -24.51283580621364067, 0.6167428607019886933 ) ) ;
#51189=CARTESIAN_POINT ( 'NONE',  ( -95.50514233772729256, -24.73486907724918282, 1.287355809206966128 ) ) ;
#51190=CARTESIAN_POINT ( 'NONE',  ( -99.62355594549717352, -24.66019654487200086, 8.947790411086115725 ) ) ;
#51191=CARTESIAN_POINT ( 'NONE',  ( 4.555389213293416617, -20.86945110937667280, 11.49999999999999645 ) ) ;
#51195=CARTESIAN_POINT ( 'NONE',  ( 18.30470771955606679, 12.64531542519679697, -1.500000000000002220 ) ) ;
#51196=CARTESIAN_POINT ( 'NONE',  ( -6.067718162532647064, 19.77315050736717694, -1.500000000000002220 ) ) ;
#51200=CARTESIAN_POINT ( 'NONE',  ( -81.52287095715006160, -24.65952944569304606, 1.056160979905698794 ) ) ;
#51201=VERTEX_POINT ( 'NONE', #79003 ) ;
#51202=B_SPLINE_CURVE_WITH_KNOTS ( 'NONE', 3,
 ( #9464, #47038, #8467, #78964 ),
 .UNSPECIFIED., .F., .F.,
 ( 4, 4 ),
 ( 1.387778780781445676E-17, 0.0001000000000000028779 ),
 .UNSPECIFIED. ) ;
#51203=CARTESIAN_POINT ( 'NONE',  ( -2.368302597431856782, 20.80102113048726409, -1.500000000000002220 ) ) ;
#51204=CARTESIAN_POINT ( 'NONE',  ( 6.492371748702247203, -20.92784845389783399, 11.49999999999999645 ) ) ;
#51205=EDGE_CURVE ( 'NONE', #47480, #59988, #32843, .T. ) ;
#51206=CARTESIAN_POINT ( 'NONE',  ( -89.58585360431281686, -24.51419770103157703, 9.386484678747175181 ) ) ;
#51207=CARTESIAN_POINT ( 'NONE',  ( -16.74547196562220464, 15.07928529822544661, 11.49999999999998934 ) ) ;
#51208=CARTESIAN_POINT ( 'NONE',  ( 20.71091302404612833, 3.140364381853995912, 11.49999999999998934 ) ) ;
#51209=CARTESIAN_POINT ( 'NONE',  ( -92.55472525529691552, -23.96169478059712787, 10.65365249895717525 ) ) ;
#51210=CARTESIAN_POINT ( 'NONE',  ( -106.5228709571500758, -23.47596703998600631, 11.44779298504228038 ) ) ;
#51211=CARTESIAN_POINT ( 'NONE',  ( -119.5211651280569924, -23.73791477778912551, 11.05961554403169878 ) ) ;
#51214=ORIENTED_EDGE ( 'NONE', *, *, #14916, .F. ) ;
#51215=ORIENTED_EDGE ( 'NONE', *, *, #17363, .F. ) ;
#51216=DIRECTION ( 'NONE',  ( 3.773278334444167608E-23, -1.000000000000000000, 0.000000000000000000 ) ) ;
#51217=CARTESIAN_POINT ( 'NONE',  ( -20.40864349294084334, -6.676163967499375573, -1.500000000000002220 ) ) ;
#51219=DIRECTION ( 'NONE',  ( -1.000000000000000000, -3.773278334444166432E-23, -8.201307841325785021E-29 ) ) ;
#51221=CARTESIAN_POINT ( 'NONE',  ( -14.90395405082875335, 14.90835605916499418, -1.500000000000002220 ) ) ;
#51224=CARTESIAN_POINT ( 'NONE',  ( -50.55077666165203709, -24.15602025860895097, 10.28564288303536856 ) ) ;
#51226=FACE_OUTER_BOUND ( 'NONE', #53815, .T. ) ;
#51227=CARTESIAN_POINT ( 'NONE',  ( 17.94654606563480215, 12.89224558282342947, -1.500000000000002220 ) ) ;
#51230=CARTESIAN_POINT ( 'NONE',  ( -44.62287095715004881, -24.65952944569303895, 1.056160979905693686 ) ) ;
#51231=CARTESIAN_POINT ( 'NONE',  ( -94.52287095715006160, -24.65952944569304961, 1.056160979905700570 ) ) ;
#51232=VECTOR ( 'NONE', #83691, 1000.000000000000114 ) ;
#51233=CARTESIAN_POINT ( 'NONE',  ( -81.88534077628074215, -29.50249666744127808, 6.293933732382250845 ) ) ;
#51234=CARTESIAN_POINT ( 'NONE',  ( 13.34776491790984210, -16.67230741956907991, 11.49999999999998934 ) ) ;
#51235=CARTESIAN_POINT ( 'NONE',  ( -113.5562042904834072, -23.48786465467241769, 11.44779295918254292 ) ) ;
#51237=PLANE ( 'NONE',  #81075 ) ;
#51240=CARTESIAN_POINT ( 'NONE',  ( -18.78231125015805958, 12.62931641965373153, -1.500000000000002220 ) ) ;
#51244=DIRECTION ( 'NONE',  ( -3.773278334453080206E-23, 0.9999999999976377785, 2.173523156925979975E-06 ) ) ;
#51245=CARTESIAN_POINT ( 'NONE',  ( -79.52213164415213953, -23.48783264082476308, -1.443836473390096575 ) ) ;
#51246=CARTESIAN_POINT ( 'NONE',  ( -19.57314199983870751, -2.777824058246878280, 11.49999999999999645 ) ) ;
#51249=CARTESIAN_POINT ( 'NONE',  ( -67.53678271749727458, -24.65952944569304606, 1.056160979905700570 ) ) ;
#51250=B_SPLINE_CURVE_WITH_KNOTS ( 'NONE', 3,
 ( #6593, #53782, #68498, #92821 ),
 .UNSPECIFIED., .F., .F.,
 ( 4, 4 ),
 ( 0.000000000000000000, 1.000000000000000000 ),
 .UNSPECIFIED. ) ;
#51252=AXIS2_PLACEMENT_3D ( 'NONE', #6179, #21387, #91910 ) ;
#51253=CARTESIAN_POINT ( 'NONE',  ( -54.52287095715006870, -29.50248528299804818, 1.056150453629033370 ) ) ;
#51254=CARTESIAN_POINT ( 'NONE',  ( -29.31644179857717347, -25.26026486303936025, 2.549173870068830006 ) ) ;
#51255=LINE ( 'NONE', #34536, #82058 ) ;
#51256=CARTESIAN_POINT ( 'NONE',  ( -16.79864850723062020, -13.61054813162024679, -1.500000000000002220 ) ) ;
#51259=CARTESIAN_POINT ( 'NONE',  ( -11.15089393765527959, -15.82809448842462885, -1.500000000000002220 ) ) ;
#51260=B_SPLINE_CURVE_WITH_KNOTS ( 'NONE', 3,
 ( #58441, #75139, #5630, #51821, #81761, #42227 ),
 .UNSPECIFIED., .F., .F.,
 ( 4, 2, 4 ),
 ( 0.000000000000000000, 0.001380764517854760412, 0.002761529035709520824 ),
 .UNSPECIFIED. ) ;
#51263=CARTESIAN_POINT ( 'NONE',  ( -2.602694502683683631, -19.63732897141692391, 11.49999999999998934 ) ) ;
#51265=CARTESIAN_POINT ( 'NONE',  ( -3.898967980886277829, 19.90457959416237088, 11.49999999999999645 ) ) ;
#51268=VERTEX_POINT ( 'NONE', #4893 ) ;
#51269=CARTESIAN_POINT ( 'NONE',  ( -110.5228709571500616, -24.99132157543167310, 2.256160258750667502 ) ) ;
#51274=CARTESIAN_POINT ( 'NONE',  ( -13.81204400269958654, 14.50282280199826701, -1.500000000000002220 ) ) ;
#51276=ORIENTED_EDGE ( 'NONE', *, *, #9825, .F. ) ;
#51278=DIRECTION ( 'NONE',  ( 7.150924204855701834E-40, 2.173523156925979975E-06, -0.9999999999976378895 ) ) ;
#51280=CARTESIAN_POINT ( 'NONE',  ( -129.5228709571500758, -24.64898659630529920, 1.056161002820834804 ) ) ;
#51282=EDGE_CURVE ( 'NONE', #39531, #72799, #81522, .T. ) ;
#51283=CARTESIAN_POINT ( 'NONE',  ( -113.5228709571500616, -24.64898659630368627, 1.056161002820831474 ) ) ;
#51284=DIRECTION ( 'NONE',  ( -3.773278334453079618E-23, 0.9999999999976377785, 2.173523156925979975E-06 ) ) ;
#51285=B_SPLINE_CURVE_WITH_KNOTS ( 'NONE', 3,
 ( #37975, #78896, #61828, #68429, #1796, #76518, #17512, #7024, #40355, #60833, #48479, #91751 ),
 .UNSPECIFIED., .F., .F.,
 ( 4, 2, 2, 2, 2, 4 ),
 ( 6.686686736723900881E-09, 0.0004767310751705819308, 0.0009534554636544272143, 0.001430179852138272444, 0.001668542046380201618, 0.001906904240622130792 ),
 .UNSPECIFIED. ) ;
#51286=CARTESIAN_POINT ( 'NONE',  ( -71.52287095715010423, -24.66019654487200086, 8.947790411086115725 ) ) ;
#51288=CARTESIAN_POINT ( 'NONE',  ( 9.809556900635294951, 17.81656380412256269, 11.49999999999998934 ) ) ;
#51291=CARTESIAN_POINT ( 'NONE',  ( -3.094460115123966570, -22.75893099265358188, 11.49999999999998934 ) ) ;
#51292=B_SPLINE_CURVE_WITH_KNOTS ( 'NONE', 3,
 ( #95921, #94918, #33523, #16791 ),
 .UNSPECIFIED., .F., .F.,
 ( 4, 4 ),
 ( 0.09985723008135170831, 0.1088636613534670478 ),
 .UNSPECIFIED. ) ;
#51293=CARTESIAN_POINT ( 'NONE',  ( -32.57492585626526704, -24.65952944569304606, 1.056160979905696351 ) ) ;
#51294=ORIENTED_EDGE ( 'NONE', *, *, #12249, .F. ) ;
#51295=DIRECTION ( 'NONE',  ( 0.000000000000000000, -2.173523156925980399E-06, 0.9999999999976378895 ) ) ;
#51296=AXIS2_PLACEMENT_3D ( 'NONE', #41157, #48775, #49280 ) ;
#51297=CARTESIAN_POINT ( 'NONE',  ( -77.62287095715005592, -24.64965695001468404, 8.947790433994182280 ) ) ;
#51298=LINE ( 'NONE', #82238, #54501 ) ;
#51299=CARTESIAN_POINT ( 'NONE',  ( -13.45780860896912934, -16.40347334334247265, 11.49999999999999645 ) ) ;
#51301=VERTEX_POINT ( 'NONE', #11005 ) ;
#51302=CARTESIAN_POINT ( 'NONE',  ( -18.12599551585701008, -12.76988789260850332, -1.500000000000002220 ) ) ;
#51303=CARTESIAN_POINT ( 'NONE',  ( -3.210669876418242197, 20.33209092710186638, 11.49999999999998934 ) ) ;
#51305=EDGE_LOOP ( 'NONE', ( #40065, #51825, #84510, #1919 ) ) ;
#51306=ORIENTED_EDGE ( 'NONE', *, *, #69404, .F. ) ;
#51307=CARTESIAN_POINT ( 'NONE',  ( -94.52287095715006160, -29.50248528299804818, 1.056150453629040253 ) ) ;
#51308=PLANE ( 'NONE',  #61596 ) ;
#51310=VECTOR ( 'NONE', #4276, 1000.000000000000114 ) ;
#51315=CARTESIAN_POINT ( 'NONE',  ( -28.62972572368664714, -24.36142566672730325, 9.386484685950513551 ) ) ;
#51316=PLANE ( 'NONE',  #14705 ) ;
#51317=CARTESIAN_POINT ( 'NONE',  ( -0.3852054317258338245, -20.75737367715079174, -1.500000000000002220 ) ) ;
#51318=CARTESIAN_POINT ( 'NONE',  ( 18.41774212405765709, -11.57998961627671441, 11.49999999999999645 ) ) ;
#51320=CARTESIAN_POINT ( 'NONE',  ( -40.45231480346743069, -25.27806139640134120, 5.081397595443370996 ) ) ;
#51321=DIRECTION ( 'NONE',  ( -3.773278334453080206E-23, 0.9999999999976377785, 2.173523156925979975E-06 ) ) ;
#51322=CARTESIAN_POINT ( 'NONE',  ( -115.5516351120022591, -24.73486907724918282, 1.287355809206964352 ) ) ;
#51323=CARTESIAN_POINT ( 'NONE',  ( -17.72129891523481149, -13.73837202384828515, -1.500000000000002220 ) ) ;
#51324=DIRECTION ( 'NONE',  ( -3.773278334453080206E-23, 0.9999999999976377785, 2.173523156925979975E-06 ) ) ;
#51326=ORIENTED_EDGE ( 'NONE', *, *, #5495, .T. ) ;
#51329=CARTESIAN_POINT ( 'NONE',  ( -86.52287095715006160, -23.48783264083431277, -1.443836473375255336 ) ) ;
#51330=ORIENTED_EDGE ( 'NONE', *, *, #13785, .T. ) ;
#51331=B_SPLINE_CURVE_WITH_KNOTS ( 'NONE', 3,
 ( #86988, #72782, #94098, #55558 ),
 .UNSPECIFIED., .F., .F.,
 ( 4, 4 ),
 ( 0.000000000000000000, 9.999999999997510880E-05 ),
 .UNSPECIFIED. ) ;
#51334=ADVANCED_FACE ( 'NONE', ( #49083 ), #20107, .F. ) ;
#51335=ORIENTED_EDGE ( 'NONE', *, *, #65704, .T. ) ;
#51336=CARTESIAN_POINT ( 'NONE',  ( -20.61954105445765251, -5.431428859615135885, -1.500000000000002220 ) ) ;
#51337=B_SPLINE_CURVE_WITH_KNOTS ( 'NONE', 3,
 ( #71069, #77653, #9665, #70055 ),
 .UNSPECIFIED., .F., .F.,
 ( 4, 4 ),
 ( 0.000000000000000000, 9.999999999996123101E-05 ),
 .UNSPECIFIED. ) ;
#51338=ORIENTED_EDGE ( 'NONE', *, *, #94608, .T. ) ;
#51340=CARTESIAN_POINT ( 'NONE',  ( 8.107222467604051630, 20.28165043084963060, 11.49999999999998934 ) ) ;
#51342=CARTESIAN_POINT ( 'NONE',  ( 4.020035926878589905, 22.33396232419688587, 11.49999999999998934 ) ) ;
#51343=CARTESIAN_POINT ( 'NONE',  ( -112.5895376238167245, -24.65952944569305316, 1.056160979905713670 ) ) ;
#51344=CARTESIAN_POINT ( 'NONE',  ( -49.52287095715004028, -23.73934037231756022, 11.05740245334329153 ) ) ;
#51345=CARTESIAN_POINT ( 'NONE',  ( 19.17116566557315949, -10.70166234769870961, -1.500000000000002220 ) ) ;
#51346=DIRECTION ( 'NONE',  ( 0.000000000000000000, -0.9999999999976377785, -2.173523156925979975E-06 ) ) ;
#51349=CARTESIAN_POINT ( 'NONE',  ( -84.52287095715006160, -29.50250243563736774, 8.947779886222141599 ) ) ;
#51352=DIRECTION ( 'NONE',  ( -3.773278334453080206E-23, 0.9999999999976377785, 2.173523156925979975E-06 ) ) ;
#51355=CARTESIAN_POINT ( 'NONE',  ( -0.1490770655183800975, -21.12008023607309681, -1.443836447538997314 ) ) ;
#51356=CARTESIAN_POINT ( 'NONE',  ( -13.59518820711925358, -16.35513075224449864, 11.49999999999998934 ) ) ;
#51357=CARTESIAN_POINT ( 'NONE',  ( -112.5905343604989923, -24.15543982623908192, -0.2315651400026420559 ) ) ;
#51358=CARTESIAN_POINT ( 'NONE',  ( -26.21213932664330670, -24.75186287970886667, 3.737064058008186418 ) ) ;
#51360=DIRECTION ( 'NONE',  ( -0.2007054744626894649, 0.000000000000000000, 0.9796516281417116945 ) ) ;
#51361=PLANE ( 'NONE',  #57336 ) ;
#51362=B_SPLINE_SURFACE_WITH_KNOTS ( 'NONE', 3, 3, ( 
 ( #88698, #65880, #19166, #27786 ),
 ( #58739, #95798, #50135, #43022 ),
 ( #27294, #89688, #50628, #18669 ),
 ( #82071, #12557, #80078, #73966 ),
 ( #97790, #41523, #26292, #88198 ),
 ( #33903, #81582, #4464, #77912 ),
 ( #23196, #61789, #76980, #54181 ) ),
 .UNSPECIFIED., .F., .F., .F.,
 ( 4, 3, 4 ),
 ( 4, 4 ),
 ( 0.0004766839783824310508, 0.1029713700210899002, 0.2054660560637973643 ),
 ( 0.2595600248839645130, 0.2606925099585566397 ),
 .UNSPECIFIED. ) ;
#51363=CARTESIAN_POINT ( 'NONE',  ( -117.5188394651187167, -24.15620529776629510, 10.23563542870659582 ) ) ;
#51364=VERTEX_POINT ( 'NONE', #2911 ) ;
#51365=CARTESIAN_POINT ( 'NONE',  ( 19.09806219120973125, -4.162641619376711510, 11.49999999999999645 ) ) ;
#51366=CARTESIAN_POINT ( 'NONE',  ( -66.62287095715002749, -24.35013146730203459, 9.818937971375113705 ) ) ;
#51367=CARTESIAN_POINT ( 'NONE',  ( -29.81175120719462157, -25.24633111994858581, 4.942810988825437235 ) ) ;
#51370=EDGE_CURVE ( 'NONE', #17140, #30450, #76905, .T. ) ;
#51371=CARTESIAN_POINT ( 'NONE',  ( -101.5228709571500758, -24.64965694238407323, 8.947790433994194714 ) ) ;
#51373=CARTESIAN_POINT ( 'NONE',  ( -27.61217026053484958, -24.64375301970309806, 8.250468979048056539 ) ) ;
#51375=CARTESIAN_POINT ( 'NONE',  ( 16.13486940644654766, 11.28601765141728741, 11.49999999999998934 ) ) ;
#51378=CARTESIAN_POINT ( 'NONE',  ( -72.62287095715005592, -29.50247984919015209, -1.443849546365055359 ) ) ;
#51381=ORIENTED_EDGE ( 'NONE', *, *, #55274, .F. ) ;
#51383=CARTESIAN_POINT ( 'NONE',  ( -45.62287095715005592, -24.92604778743018556, 8.074972756849359001 ) ) ;
#51384=CARTESIAN_POINT ( 'NONE',  ( -55.56003731193040807, -23.85016227208578954, -0.8807180028928371929 ) ) ;
#51385=CARTESIAN_POINT ( 'NONE',  ( -63.22287095715004313, -23.47593901973090524, -1.443836447538997536 ) ) ;
#51386=CARTESIAN_POINT ( 'NONE',  ( -31.62287095715005236, -23.95044443724991368, 10.65354141964649948 ) ) ;
#51388=AXIS2_PLACEMENT_3D ( 'NONE', #84396, #99601, #55459 ) ;
#51389=DIRECTION ( 'NONE',  ( 0.000000000000000000, -0.9999999999976377785, -2.173523156925979975E-06 ) ) ;
#51391=CARTESIAN_POINT ( 'NONE',  ( -107.6280297884409265, -24.15543982623907837, -0.2315651400026443874 ) ) ;
#51392=CARTESIAN_POINT ( 'NONE',  ( 19.82558669001425500, -2.195561414069463702, 11.49999999999998934 ) ) ;
#51394=DIRECTION ( 'NONE',  ( -3.773278334453079618E-23, 0.9999999999976377785, 2.173523156925979975E-06 ) ) ;
#51395=CARTESIAN_POINT ( 'NONE',  ( -0.03888317010184255684, -22.54662680705505551, 8.463919116204994708 ) ) ;
#51396=ORIENTED_EDGE ( 'NONE', *, *, #44976, .T. ) ;
#51397=DIRECTION ( 'NONE',  ( -3.773278334453079618E-23, 0.9999999999976377785, 2.173523156925979975E-06 ) ) ;
#51399=PLANE ( 'NONE',  #71841 ) ;
#51401=FACE_OUTER_BOUND ( 'NONE', #73789, .T. ) ;
#51404=B_SPLINE_CURVE_WITH_KNOTS ( 'NONE', 3,
 ( #19637, #13516, #5418, #67329 ),
 .UNSPECIFIED., .F., .F.,
 ( 4, 4 ),
 ( 0.000000000000000000, 1.000000000000000000 ),
 .UNSPECIFIED. ) ;
#51405=ORIENTED_EDGE ( 'NONE', *, *, #49017, .F. ) ;
#51406=CARTESIAN_POINT ( 'NONE',  ( -97.52287095715007581, -23.47593901973090524, -1.443836447538996648 ) ) ;
#51409=ORIENTED_EDGE ( 'NONE', *, *, #20418, .F. ) ;
#51410=CARTESIAN_POINT ( 'NONE',  ( 3.706880958665978998, 19.89330832657401515, -1.500000000000002220 ) ) ;
#51411=B_SPLINE_CURVE_WITH_KNOTS ( 'NONE', 3,
 ( #8285, #95024, #86908, #9786 ),
 .UNSPECIFIED., .F., .F.,
 ( 4, 4 ),
 ( 2.775557561562891351E-17, 8.203124999998923084E-05 ),
 .UNSPECIFIED. ) ;
#51413=EDGE_CURVE ( 'NONE', #7766, #68548, #92545, .T. ) ;
#51417=CARTESIAN_POINT ( 'NONE',  ( -58.52287095715004739, -23.47593901973090169, -1.443836447538997092 ) ) ;
#51418=ORIENTED_EDGE ( 'NONE', *, *, #62512, .F. ) ;
#51419=CARTESIAN_POINT ( 'NONE',  ( -105.9228709571500673, -23.47596703998600631, 11.44779298504227860 ) ) ;
#51421=CARTESIAN_POINT ( 'NONE',  ( 20.03642891561555928, 0.6179553080306146029, -1.500000000000002220 ) ) ;
#51422=CARTESIAN_POINT ( 'NONE',  ( 19.54352652498339182, 7.673529024697476331, 11.49999999999999645 ) ) ;
#51424=CARTESIAN_POINT ( 'NONE',  ( -28.94471403569382773, -25.05935760451456318, 6.779848816579228554 ) ) ;
#51425=CARTESIAN_POINT ( 'NONE',  ( -111.6228709571500417, -24.50321055353806088, 9.387540953477531147 ) ) ;
#51426=CARTESIAN_POINT ( 'NONE',  ( -21.42919730060085115, -5.301375089729956969, 11.49999999999998934 ) ) ;
#51427=B_SPLINE_CURVE_WITH_KNOTS ( 'NONE', 3,
 ( #45543, #24185, #77461, #7961 ),
 .UNSPECIFIED., .F., .F.,
 ( 4, 4 ),
 ( 0.000000000000000000, 9.999999999998897304E-05 ),
 .UNSPECIFIED. ) ;
#51428=CARTESIAN_POINT ( 'NONE',  ( -66.55620429048339304, -24.66019654487199020, 8.947790411086131712 ) ) ;
#51429=CARTESIAN_POINT ( 'NONE',  ( -47.62287095715004881, -24.64898659630367916, 1.056161002820821038 ) ) ;
#51430=CARTESIAN_POINT ( 'NONE',  ( -50.30027857337484676, -25.27344760046473482, 3.296100333510875391 ) ) ;
#51431=ORIENTED_EDGE ( 'NONE', *, *, #55153, .T. ) ;
#51433=CARTESIAN_POINT ( 'NONE',  ( -31.56131489220916819, -23.73766607897669800, -1.055555164236445131 ) ) ;
#51434=ORIENTED_EDGE ( 'NONE', *, *, #28038, .T. ) ;
#51438=CARTESIAN_POINT ( 'NONE',  ( -76.55419634045316002, -23.96119346886880663, -0.6495511937832058047 ) ) ;
#51439=CARTESIAN_POINT ( 'NONE',  ( -16.28974412851428255, -12.55652860423730388, -1.500000000000002220 ) ) ;
#51440=CARTESIAN_POINT ( 'NONE',  ( -19.30636564405121902, 9.640216152154000184, 11.49999999999999645 ) ) ;
#51441=ORIENTED_EDGE ( 'NONE', *, *, #6831, .F. ) ;
#51442=CARTESIAN_POINT ( 'NONE',  ( -50.26609345566524922, -25.13378748658239559, 7.097951806649573037 ) ) ;
#51443=CARTESIAN_POINT ( 'NONE',  ( -99.12672354517025042, -25.27198829872966712, 4.094481813589349706 ) ) ;
#51444=PLANE ( 'NONE',  #22110 ) ;
#51445=CARTESIAN_POINT ( 'NONE',  ( 4.697571063781373013, 21.84268702631108994, 11.49999999999998934 ) ) ;
#51446=VECTOR ( 'NONE', #91788, 1000.000000000000114 ) ;
#51447=CARTESIAN_POINT ( 'NONE',  ( -50.62287095715004170, -23.48783264082478084, -1.443836473390070596 ) ) ;
#51452=CARTESIAN_POINT ( 'NONE',  ( 17.92008016455634589, 10.74458801173053324, 11.49999999999998934 ) ) ;
#51453=ORIENTED_EDGE ( 'NONE', *, *, #29385, .T. ) ;
#51454=FACE_OUTER_BOUND ( 'NONE', #35363, .T. ) ;
#51455=ORIENTED_EDGE ( 'NONE', *, *, #91076, .T. ) ;
#51457=ORIENTED_EDGE ( 'NONE', *, *, #90424, .T. ) ;
#51459=CARTESIAN_POINT ( 'NONE',  ( -100.5576076336107434, -23.85049219812686161, 10.88485053497527133 ) ) ;
#51460=CARTESIAN_POINT ( 'NONE',  ( -3.482456173223098528, 20.84670800329844198, -1.500000000000002220 ) ) ;
#51461=ORIENTED_EDGE ( 'NONE', *, *, #79934, .F. ) ;
#51464=CARTESIAN_POINT ( 'NONE',  ( -129.5895376238167387, -23.48786465467241769, 11.44779295918253581 ) ) ;
#51466=PLANE ( 'NONE',  #90704 ) ;
#51468=CARTESIAN_POINT ( 'NONE',  ( -21.74948284930419717, -1.071797830193938372, -1.500000000000002220 ) ) ;
#51469=CARTESIAN_POINT ( 'NONE',  ( -107.5228709571501042, -23.48783264083360578, -1.443836473376361118 ) ) ;
#51470=CARTESIAN_POINT ( 'NONE',  ( -7.140196579304709523, 21.16591527347414115, 11.49999999999999645 ) ) ;
#51472=CARTESIAN_POINT ( 'NONE',  ( -57.52287095715005449, -23.48786465467241058, 11.44779295918254824 ) ) ;
#51474=CARTESIAN_POINT ( 'NONE',  ( -106.5228709571500900, -24.33927499327855060, 9.819080762295804732 ) ) ;
#51476=ORIENTED_EDGE ( 'NONE', *, *, #67681, .T. ) ;
#51477=ORIENTED_EDGE ( 'NONE', *, *, #40103, .T. ) ;
#51479=CARTESIAN_POINT ( 'NONE',  ( -86.58953762381669605, -23.47596703998600631, 11.44779298504227683 ) ) ;
#51481=CARTESIAN_POINT ( 'NONE',  ( -43.62287095715004881, -24.64965695001467694, 8.947790433994187609 ) ) ;
#51482=EDGE_CURVE ( 'NONE', #45115, #46021, #23518, .T. ) ;
#51483=CARTESIAN_POINT ( 'NONE',  ( -87.52287095715006160, -24.33927499327855770, 9.819080762295810061 ) ) ;
#51484=B_SPLINE_CURVE_WITH_KNOTS ( 'NONE', 3,
 ( #55001, #40269, #64131, #85940 ),
 .UNSPECIFIED., .F., .F.,
 ( 4, 4 ),
 ( 0.000000000000000000, 1.000000000000000000 ),
 .UNSPECIFIED. ) ;
#51485=CARTESIAN_POINT ( 'NONE',  ( -36.52287095715009002, -24.66019654487199730, 8.947790411086124607 ) ) ;
#51487=CARTESIAN_POINT ( 'NONE',  ( 14.41255161864883583, -12.98630880007775268, 11.49999999999999645 ) ) ;
#51489=ORIENTED_EDGE ( 'NONE', *, *, #80045, .T. ) ;
#51492=EDGE_CURVE ( 'NONE', #67443, #36561, #63648, .T. ) ;
#51494=EDGE_CURVE ( 'NONE', #31671, #48067, #70281, .T. ) ;
#51497=CARTESIAN_POINT ( 'NONE',  ( -36.52287095715006870, -23.96177878511308279, 10.65340807706330573 ) ) ;
#51498=CARTESIAN_POINT ( 'NONE',  ( 10.47639735327893362, 16.54961352017854637, 11.49999999999998934 ) ) ;
#51499=B_SPLINE_SURFACE_WITH_KNOTS ( 'NONE', 3, 1, ( 
 ( #47392, #45896 ),
 ( #30155, #61128 ),
 ( #76319, #77809 ),
 ( #78319, #86445 ),
 ( #23524, #8825 ),
 ( #39762, #70724 ),
 ( #31154, #92056 ),
 ( #54503, #7819 ),
 ( #6818, #92551 ),
 ( #77318, #85437 ),
 ( #1218, #23023 ),
 ( #32152, #38764 ),
 ( #63127, #15923 ),
 ( #94053, #22527 ),
 ( #24539, #55509 ),
 ( #53520, #46891 ),
 ( #84443, #76813 ),
 ( #38266, #69224 ),
 ( #8321, #100139 ) ),
 .UNSPECIFIED., .F., .F., .F.,
 ( 4, 1, 1, 1, 1, 1, 1, 1, 1, 1, 1, 1, 1, 1, 1, 1, 4 ),
 ( 2, 2 ),
 ( 0.000000000000000000, 0.06879079439061809575, 0.1351032894311278987, 0.1989786743106516376, 0.2619042997808557205, 0.3234949693679702309, 0.3851953779660500787, 0.4469692387407731005, 0.5097647767031340260, 0.5722505688473688013, 0.6334051756611546180, 0.6932511629217514848, 0.7525831627856720552, 0.8125792661534239070, 0.8732750849201905696, 0.9355499428950290186, 1.000000000000000000 ),
 ( 0.000000000000000000, 1.000000000000000000 ),
 .UNSPECIFIED. ) ;
#51500=CARTESIAN_POINT ( 'NONE',  ( -66.62287095715005592, -23.48786465467241058, 11.44779295918254647 ) ) ;
#51502=EDGE_CURVE ( 'NONE', #62579, #5690, #53750, .T. ) ;
#51503=CARTESIAN_POINT ( 'NONE',  ( 18.51311748589099082, 11.02308708543723270, -1.500000000000002220 ) ) ;
#51504=CARTESIAN_POINT ( 'NONE',  ( -56.52287095715006870, -24.64898659630367916, 1.056161002820822592 ) ) ;
#51505=CARTESIAN_POINT ( 'NONE',  ( -70.51930845923730828, -25.12219141572745684, 7.087032725586937865 ) ) ;
#51506=DIRECTION ( 'NONE',  ( -3.773278334453080206E-23, 0.9999999999976377785, 2.173523156925979975E-06 ) ) ;
#51507=CARTESIAN_POINT ( 'NONE',  ( -99.52764846858842418, -25.27473375014014678, 3.999772248440511824 ) ) ;
#51508=CARTESIAN_POINT ( 'NONE',  ( -21.75629724252761577, 7.406401271465676395, -1.500000000000002220 ) ) ;
#51510=CARTESIAN_POINT ( 'NONE',  ( -49.52287095715006160, -24.64965694238406613, 8.947790433994203596 ) ) ;
#51512=CARTESIAN_POINT ( 'NONE',  ( -5.623992922573770592, 19.38241096367466199, 11.49999999999999645 ) ) ;
#51513=CARTESIAN_POINT ( 'NONE',  ( -109.2412217894342916, -25.10927504460140725, 3.330161293093501396 ) ) ;
#51514=CARTESIAN_POINT ( 'NONE',  ( -91.52287095715009002, -23.73907113216989728, -1.053371485793250129 ) ) ;
#51516=CARTESIAN_POINT ( 'NONE',  ( -104.5562042904834215, -24.65952944569305316, 1.056160979905702568 ) ) ;
#51517=CARTESIAN_POINT ( 'NONE',  ( -121.6228709571500417, -24.65952944569305316, 1.056160979905705677 ) ) ;
#51518=FACE_OUTER_BOUND ( 'NONE', #32349, .T. ) ;
#51519=CARTESIAN_POINT ( 'NONE',  ( -19.70454523906213495, -2.556213046838741842, -1.500000000000002220 ) ) ;
#51521=CARTESIAN_POINT ( 'NONE',  ( -113.5144507812068753, -24.65952944569304606, 1.056160979905704789 ) ) ;
#51522=CARTESIAN_POINT ( 'NONE',  ( 19.74453702311487646, -0.1846442961375113490, -1.500000000000002220 ) ) ;
#51523=VECTOR ( 'NONE', #21037, 1000.000000000000114 ) ;
#51524=CARTESIAN_POINT ( 'NONE',  ( -126.5896042291024202, -24.35071581493544457, 9.817618358456011052 ) ) ;
#51526=DIRECTION ( 'NONE',  ( 0.000000000000000000, -2.173523156925979552E-06, 0.9999999999976378895 ) ) ;
#51527=CARTESIAN_POINT ( 'NONE',  ( -7.851838630353038972, -19.11370409007043847, 11.49999999999999645 ) ) ;
#51528=CARTESIAN_POINT ( 'NONE',  ( -53.58953762381672448, -24.66019654487199020, 8.947790411086131712 ) ) ;
#51529=EDGE_CURVE ( 'NONE', #38437, #43756, #44027, .T. ) ;
#51532=CARTESIAN_POINT ( 'NONE',  ( -22.63693132222386950, 1.387278323242118416, 11.49999999999999645 ) ) ;
#51535=EDGE_CURVE ( 'NONE', #70943, #98477, #99717, .T. ) ;
#51536=CARTESIAN_POINT ( 'NONE',  ( -62.58953762381672448, -23.47593901973091235, -1.443836447539007972 ) ) ;
#51537=AXIS2_PLACEMENT_3D ( 'NONE', #80809, #73204, #11292 ) ;
#51538=CARTESIAN_POINT ( 'NONE',  ( -63.49532551922489176, -24.51314013834316796, 0.6176544820404160641 ) ) ;
#51539=ADVANCED_FACE ( 'NONE', ( #1275 ), #8877, .T. ) ;
#51543=VERTEX_POINT ( 'NONE', #24590 ) ;
#51545=CARTESIAN_POINT ( 'NONE',  ( -6.237877366497927234, -22.00199818733190327, -1.500000000000002220 ) ) ;
#51547=EDGE_CURVE ( 'NONE', #31857, #85110, #94881, .T. ) ;
#51548=CARTESIAN_POINT ( 'NONE',  ( -13.01863397230089170, 17.21462230531794901, -1.500000000000002220 ) ) ;
#51550=CARTESIAN_POINT ( 'NONE',  ( -113.5871604955099059, -24.66019654487200086, 8.947790411086106843 ) ) ;
#51551=CARTESIAN_POINT ( 'NONE',  ( -32.55620429048340014, -23.48783264082478084, -1.443836473390075037 ) ) ;
#51552=CARTESIAN_POINT ( 'NONE',  ( 4.940617368476682536, -22.01678987175928981, 11.49999999999999645 ) ) ;
#51553=VERTEX_POINT ( 'NONE', #8374 ) ;
#51554=CARTESIAN_POINT ( 'NONE',  ( -43.52287095715005449, -23.96127896942127933, -0.6493128930940295085 ) ) ;
#51555=CARTESIAN_POINT ( 'NONE',  ( 17.26801960494244881, -13.64313956103151071, 11.49999999999998934 ) ) ;
#51556=CARTESIAN_POINT ( 'NONE',  ( -64.52287095715006160, -24.50216790748205398, 0.6166512839542503954 ) ) ;
#51557=CARTESIAN_POINT ( 'NONE',  ( -41.58766378979927936, -25.10925883918385537, 3.364589983749641799 ) ) ;
#51558=EDGE_LOOP ( 'NONE', ( #30483, #10273, #15103, #27225, #55284, #45632 ) ) ;
#51560=PLANE ( 'NONE',  #81611 ) ;
#51561=CARTESIAN_POINT ( 'NONE',  ( -90.62479060358214156, -24.92592662359561473, 8.075495903018000021 ) ) ;
#51562=ORIENTED_EDGE ( 'NONE', *, *, #38024, .F. ) ;
#51566=CARTESIAN_POINT ( 'NONE',  ( -65.52287095715004739, -24.91544648472619627, 1.928969306349230806 ) ) ;
#51567=CARTESIAN_POINT ( 'NONE',  ( -92.62287095715005592, -23.48786465467241413, 11.44779295918254469 ) ) ;
#51568=CARTESIAN_POINT ( 'NONE',  ( -57.62781167713143304, -24.51314013834315375, 0.6176544820404114011 ) ) ;
#51569=CARTESIAN_POINT ( 'NONE',  ( 5.143668500415711442, -19.74887971880038151, -1.500000000000002220 ) ) ;
#51570=ORIENTED_EDGE ( 'NONE', *, *, #44414, .T. ) ;
#51572=CARTESIAN_POINT ( 'NONE',  ( -105.5497180537893200, -24.63355581998386867, 0.9682620441943899925 ) ) ;
#51573=PLANE ( 'NONE',  #17266 ) ;
#51574=ORIENTED_EDGE ( 'NONE', *, *, #34775, .F. ) ;
#51575=CARTESIAN_POINT ( 'NONE',  ( -100.5228709571500616, -23.47596703998600631, 11.44779298504228215 ) ) ;
#51576=CARTESIAN_POINT ( 'NONE',  ( -27.99827674658315502, -24.63646060442122732, 8.232207369485870174 ) ) ;
#51578=CARTESIAN_POINT ( 'NONE',  ( 1.081820405348005165, -20.78239343107542680, 11.49999999999998934 ) ) ;
#51580=CARTESIAN_POINT ( 'NONE',  ( -101.5985593676237499, -23.48783264082477018, -1.443836473390089248 ) ) ;
#51581=VERTEX_POINT ( 'NONE', #71281 ) ;
#51582=B_SPLINE_CURVE_WITH_KNOTS ( 'NONE', 3,
 ( #38445, #69397, #31841, #71407 ),
 .UNSPECIFIED., .F., .F.,
 ( 4, 4 ),
 ( 0.000000000000000000, 0.0001000000000000028644 ),
 .UNSPECIFIED. ) ;
#51583=B_SPLINE_SURFACE_WITH_KNOTS ( 'NONE', 3, 1, ( 
 ( #60566, #92481 ),
 ( #22953, #5759 ),
 ( #91988, #76743 ),
 ( #7244, #22459 ),
 ( #53447, #15355 ),
 ( #90992, #20973 ),
 ( #53945, #21963 ),
 ( #84874, #46320 ),
 ( #98599, #76255 ),
 ( #5260, #91484 ),
 ( #84375, #82874 ),
 ( #13360, #75265 ),
 ( #71667, #7753 ),
 ( #64076, #54941 ),
 ( #85882, #8763 ),
 ( #71165, #31084 ),
 ( #17873, #23971 ),
 ( #9250, #32592 ),
 ( #16360, #39699 ) ),
 .UNSPECIFIED., .F., .F., .F.,
 ( 4, 1, 1, 1, 1, 1, 1, 1, 1, 1, 1, 1, 1, 1, 1, 1, 4 ),
 ( 2, 2 ),
 ( 0.000000000000000000, 0.06420729528298517452, 0.1264246897797454694, 0.1876802842649225589, 0.2482164244552149956, 0.3083050600086130189, 0.3696609913251429069, 0.4316985517867830136, 0.4959468922087650333, 0.5597580239721172690, 0.6222954078261602184, 0.6839106352841730629, 0.7450924080566231344, 0.8067402253892927977, 0.8690866181212024699, 0.9332900029747993598, 1.000000000000000000 ),
 ( 0.000000000000000000, 1.000000000000000000 ),
 .UNSPECIFIED. ) ;
#51588=CARTESIAN_POINT ( 'NONE',  ( -78.62287095715005592, -24.51283580621364777, 0.6167428607019836972 ) ) ;
#51589=CARTESIAN_POINT ( 'NONE',  ( -76.52287095715011844, -24.33927499327856125, 9.819080762295813614 ) ) ;
#51590=CARTESIAN_POINT ( 'NONE',  ( -52.62287095715004881, -23.96177878511308634, 10.65340807706330217 ) ) ;
#51591=CARTESIAN_POINT ( 'NONE',  ( -71.20303962927951602, -25.24515144792784227, 5.785490083912771198 ) ) ;
#51592=CARTESIAN_POINT ( 'NONE',  ( 14.67205787815721862, 16.58792043909384262, 11.49999999999999645 ) ) ;
#51593=ORIENTED_EDGE ( 'NONE', *, *, #20604, .F. ) ;
#51594=CARTESIAN_POINT ( 'NONE',  ( -108.6261718626276149, -24.34968618360934300, 0.1864209137778971292 ) ) ;
#51595=CARTESIAN_POINT ( 'NONE',  ( 22.57354875331468591, -1.174960877787051716, -1.500000000000002220 ) ) ;
#51596=AXIS2_PLACEMENT_3D ( 'NONE', #76684, #37146, #77687 ) ;
#51597=CARTESIAN_POINT ( 'NONE',  ( -46.52287095715006160, -23.48786465467241058, 11.44779295918255002 ) ) ;
#51599=ORIENTED_EDGE ( 'NONE', *, *, #26993, .F. ) ;
#51600=CARTESIAN_POINT ( 'NONE',  ( -78.55620429048339304, -24.66019654487199730, 8.947790411086128159 ) ) ;
#51601=EDGE_CURVE ( 'NONE', #93020, #64856, #26607, .T. ) ;
#51602=CARTESIAN_POINT ( 'NONE',  ( -57.65693448539914812, -23.48786465467241058, 11.44779295918254647 ) ) ;
#51604=EDGE_CURVE ( 'NONE', #88839, #93802, #64191, .T. ) ;
#51606=CARTESIAN_POINT ( 'NONE',  ( -126.5228709571500616, -23.73907113216990084, -1.053371485793243911 ) ) ;
#51607=CARTESIAN_POINT ( 'NONE',  ( 14.63995501510512653, -16.76770752772931772, -1.500000000000002220 ) ) ;
#51610=ORIENTED_EDGE ( 'NONE', *, *, #48272, .F. ) ;
#51611=CARTESIAN_POINT ( 'NONE',  ( -110.5895376238167387, -23.48786465467241769, 11.44779295918254114 ) ) ;
#51612=LINE ( 'NONE', #15027, #79970 ) ;
#51613=DIRECTION ( 'NONE',  ( -3.773278334453080206E-23, 0.9999999999976377785, 2.173523156925979975E-06 ) ) ;
#51616=CARTESIAN_POINT ( 'NONE',  ( -108.6228709571500701, -23.96127896941633750, -0.6493128931037804863 ) ) ;
#51617=CARTESIAN_POINT ( 'NONE',  ( -63.62287095715004881, -29.50247984919015209, -1.443849546365056913 ) ) ;
#51618=CARTESIAN_POINT ( 'NONE',  ( 14.32981562401322506, -13.22600733894156200, -1.500000000000002220 ) ) ;
#51620=ADVANCED_FACE ( 'NONE', ( #73283 ), #41332, .F. ) ;
#51621=CARTESIAN_POINT ( 'NONE',  ( -15.31780299886000485, -15.04297462106122474, 11.49999999999998934 ) ) ;
#51622=CARTESIAN_POINT ( 'NONE',  ( -25.54641640974780259, -24.58000095359798820, 4.381686515786591407 ) ) ;
#51625=CARTESIAN_POINT ( 'NONE',  ( -7.631545101075025705, 21.52643039700453897, -1.500000000000002220 ) ) ;
#51627=CARTESIAN_POINT ( 'NONE',  ( -106.5141254747104824, -24.35071581493544457, 9.817618358456019934 ) ) ;
#51629=CARTESIAN_POINT ( 'NONE',  ( 13.83478396660306942, -14.44641118834825910, 11.49999999999999645 ) ) ;
#51630=FACE_OUTER_BOUND ( 'NONE', #52532, .T. ) ;
#51631=CARTESIAN_POINT ( 'NONE',  ( -57.58953762381671737, -23.48786465467241058, 11.44779295918254824 ) ) ;
#51632=CARTESIAN_POINT ( 'NONE',  ( -76.52287095715007581, -23.47596703998600631, 11.44779298504228571 ) ) ;
#51636=CARTESIAN_POINT ( 'NONE',  ( -65.52287095715010423, -24.15516710230292929, 10.28746687063725851 ) ) ;
#51637=CARTESIAN_POINT ( 'NONE',  ( 19.97611268498323511, -8.487024919450899318, -1.500000000000002220 ) ) ;
#51638=CARTESIAN_POINT ( 'NONE',  ( -60.62287095715004881, -25.00158670708908915, 2.256160236439166855 ) ) ;
#51639=CARTESIAN_POINT ( 'NONE',  ( 12.76379665850700640, 14.79237594083867080, -1.500000000000002220 ) ) ;
#51640=CARTESIAN_POINT ( 'NONE',  ( -129.5228709571500758, -29.50250786944525672, 11.44777988621622633 ) ) ;
#51641=B_SPLINE_CURVE_WITH_KNOTS ( 'NONE', 3,
 ( #23401, #54387, #11698, #65527 ),
 .UNSPECIFIED., .F., .F.,
 ( 4, 4 ),
 ( 0.000000000000000000, 0.0001000000000000028915 ),
 .UNSPECIFIED. ) ;
#51642=B_SPLINE_CURVE_WITH_KNOTS ( 'NONE', 3,
 ( #19779, #51750, #73095, #19284 ),
 .UNSPECIFIED., .F., .F.,
 ( 4, 4 ),
 ( 0.000000000000000000, 1.000000000000000000 ),
 .UNSPECIFIED. ) ;
#51646=FACE_OUTER_BOUND ( 'NONE', #3656, .T. ) ;
#51648=CARTESIAN_POINT ( 'NONE',  ( 5.889875310795558150, 19.62242631308348706, 11.49999999999999645 ) ) ;
#51650=CARTESIAN_POINT ( 'NONE',  ( -113.5562042904833788, -24.66019654487199730, 8.947790411086124607 ) ) ;
#51651=VERTEX_POINT ( 'NONE', #34223 ) ;
#51652=CARTESIAN_POINT ( 'NONE',  ( -109.4120340803280982, -25.29715050432110601, 4.545091671428740376 ) ) ;
#51653=CARTESIAN_POINT ( 'NONE',  ( -39.44687923781921057, -25.28892616455411613, 4.188173659901107904 ) ) ;
#51654=CARTESIAN_POINT ( 'NONE',  ( -127.6228709571500559, -23.47593901973091235, -1.443836447538995760 ) ) ;
#51656=CARTESIAN_POINT ( 'NONE',  ( -123.5228709571500474, -24.50321055353804311, 9.387540953477502725 ) ) ;
#51657=ORIENTED_EDGE ( 'NONE', *, *, #44272, .T. ) ;
#51661=CARTESIAN_POINT ( 'NONE',  ( -20.34888222059871410, 10.79260868881566715, 11.49999999999999645 ) ) ;
#51662=CARTESIAN_POINT ( 'NONE',  ( -21.15473383059569557, 8.456223909384457116, 11.49999999999998934 ) ) ;
#51664=CARTESIAN_POINT ( 'NONE',  ( -54.52287095715006870, -29.50247984919015209, -1.443849546365058689 ) ) ;
#51665=CARTESIAN_POINT ( 'NONE',  ( -60.72380231473932355, -25.13069340115295702, 2.947789388436138580 ) ) ;
#51667=PLANE ( 'NONE',  #17133 ) ;
#51668=CARTESIAN_POINT ( 'NONE',  ( -110.5509718465033018, -24.63355581998384380, 0.9682620441943931011 ) ) ;
#51670=CARTESIAN_POINT ( 'NONE',  ( 18.32745805453730981, -11.99952526121574259, 11.49999999999998934 ) ) ;
#51672=B_SPLINE_CURVE_WITH_KNOTS ( 'NONE', 3,
 ( #21378, #60481, #91397, #558 ),
 .UNSPECIFIED., .F., .F.,
 ( 4, 4 ),
 ( 0.000000000000000000, 1.000000000000000000 ),
 .UNSPECIFIED. ) ;
#51673=LINE ( 'NONE', #59793, #93025 ) ;
#51674=CARTESIAN_POINT ( 'NONE',  ( -103.5562042904833930, -24.65952944569304606, 1.056160979905701680 ) ) ;
#51677=B_SPLINE_CURVE_WITH_KNOTS ( 'NONE', 3,
 ( #89837, #64539, #89346, #10723, #81728, #20308 ),
 .UNSPECIFIED., .F., .F.,
 ( 4, 2, 4 ),
 ( 6.391158118969316353E-06, 0.001387004593080787881, 0.002767618028042606766 ),
 .UNSPECIFIED. ) ;
#51678=CARTESIAN_POINT ( 'NONE',  ( 20.14718400222343320, -3.498931157112906476, -1.500000000000002220 ) ) ;
#51679=VERTEX_POINT ( 'NONE', #87502 ) ;
#51680=EDGE_LOOP ( 'NONE', ( #46212, #62805, #95448, #37692 ) ) ;
#51681=ORIENTED_EDGE ( 'NONE', *, *, #73281, .F. ) ;
#51683=CARTESIAN_POINT ( 'NONE',  ( -22.27228905017084060, 5.866681652885556986, 11.49999999999998934 ) ) ;
#51685=CARTESIAN_POINT ( 'NONE',  ( 20.24638344296597836, 0.1212440198127159030, -1.500000000000002220 ) ) ;
#51686=ORIENTED_EDGE ( 'NONE', *, *, #79921, .F. ) ;
#51687=DIRECTION ( 'NONE',  ( -3.773278334444167608E-23, 1.000000000000000000, 0.000000000000000000 ) ) ;
#51689=CARTESIAN_POINT ( 'NONE',  ( -95.54323782235148599, -24.92564183028979485, 1.928384488918254425 ) ) ;
#51690=CARTESIAN_POINT ( 'NONE',  ( -53.56763007331336723, -23.48786465467240703, 11.44779295918255002 ) ) ;
#51691=CARTESIAN_POINT ( 'NONE',  ( 21.15477495681221143, 3.540436534888726783, 11.49999999999999645 ) ) ;
#51695=CARTESIAN_POINT ( 'NONE',  ( 14.63995501510512653, -16.76770752772931772, -1.500000000000002220 ) ) ;
#51696=CARTESIAN_POINT ( 'NONE',  ( 7.508984785159893427, -19.29828013722326929, -1.500000000000002220 ) ) ;
#51697=ORIENTED_EDGE ( 'NONE', *, *, #45378, .F. ) ;
#51699=CARTESIAN_POINT ( 'NONE',  ( -28.66134147976880442, -23.58502333657346028, -1.055554491438110309 ) ) ;
#51700=ORIENTED_EDGE ( 'NONE', *, *, #48454, .T. ) ;
#51702=ORIENTED_EDGE ( 'NONE', *, *, #21720, .T. ) ;
#51703=CARTESIAN_POINT ( 'NONE',  ( 20.88312143257166653, -1.666129412636018214, -1.500000000000002220 ) ) ;
#51704=CARTESIAN_POINT ( 'NONE',  ( -11.13288495942205536, 18.84158392345546318, 11.49999999999999645 ) ) ;
#51705=CARTESIAN_POINT ( 'NONE',  ( -73.64405303056334162, -23.73791477778911840, 11.05961554403170766 ) ) ;
#51706=CARTESIAN_POINT ( 'NONE',  ( -6.869692127560369066, -21.44495933931894527, -1.500000000000002220 ) ) ;
#51707=CARTESIAN_POINT ( 'NONE',  ( 17.97375762979478253, -10.76934015532128797, -1.500000000000002220 ) ) ;
#51709=CARTESIAN_POINT ( 'NONE',  ( -119.6248171011402519, -24.35071581493544457, 9.817618358456018157 ) ) ;
#51710=CARTESIAN_POINT ( 'NONE',  ( -31.24388727629348494, -29.50250091417111520, 8.247779886223803203 ) ) ;
#51712=ORIENTED_EDGE ( 'NONE', *, *, #67777, .T. ) ;
#51714=B_SPLINE_CURVE_WITH_KNOTS ( 'NONE', 3,
 ( #1097, #85829, #78692, #1604 ),
 .UNSPECIFIED., .F., .F.,
 ( 4, 4 ),
 ( 0.000000000000000000, 9.999999999999592548E-05 ),
 .UNSPECIFIED. ) ;
#51715=CARTESIAN_POINT ( 'NONE',  ( -66.65278898335940028, -23.48783264082476308, -1.443836473390097463 ) ) ;
#51716=CARTESIAN_POINT ( 'NONE',  ( -5.860608850286626925, 20.67097946995454905, -1.500000000000002220 ) ) ;
#51718=DIRECTION ( 'NONE',  ( -3.773278334453079618E-23, 0.9999999999976377785, 2.173523156925979975E-06 ) ) ;
#51719=ORIENTED_EDGE ( 'NONE', *, *, #83070, .F. ) ;
#51720=CARTESIAN_POINT ( 'NONE',  ( -13.19772682967519195, -16.48504770976277101, -1.500000000000002220 ) ) ;
#51721=CARTESIAN_POINT ( 'NONE',  ( -100.4326965455114902, -25.19502912051678578, 3.293943094755625633 ) ) ;
#51724=CARTESIAN_POINT ( 'NONE',  ( -64.57975988545082657, -24.65952944569304250, 1.056160979905695685 ) ) ;
#51726=CARTESIAN_POINT ( 'NONE',  ( -83.55442485235529659, -23.96169478059713143, 10.65365249895718058 ) ) ;
#51727=DIRECTION ( 'NONE',  ( -3.773278334453079618E-23, 0.9999999999976377785, 2.173523156925979975E-06 ) ) ;
#51728=DIRECTION ( 'NONE',  ( -0.000000000000000000, 2.173523156925979552E-06, -0.9999999999976378895 ) ) ;
#51729=CARTESIAN_POINT ( 'NONE',  ( -11.88820881604258339, -18.65297325734525913, -1.500000000000002220 ) ) ;
#51731=EDGE_CURVE ( 'NONE', #34090, #15342, #10372, .T. ) ;
#51732=CARTESIAN_POINT ( 'NONE',  ( -109.0560589239626950, -25.30235252500154175, 4.712086642211391840 ) ) ;
#51736=B_SPLINE_CURVE_WITH_KNOTS ( 'NONE', 3,
 ( #35079, #43197, #58914, #98450 ),
 .UNSPECIFIED., .F., .F.,
 ( 4, 4 ),
 ( 0.000000000000000000, 9.999999999998897304E-05 ),
 .UNSPECIFIED. ) ;
#51737=CARTESIAN_POINT ( 'NONE',  ( -100.6369790529841310, -23.85016227208580020, -0.8807180028928295323 ) ) ;
#51738=AXIS2_PLACEMENT_3D ( 'NONE', #88126, #54801, #61911 ) ;
#51739=CARTESIAN_POINT ( 'NONE',  ( -17.77321681866180469, -7.816401696202086136, -1.500000000000002220 ) ) ;
#51741=CARTESIAN_POINT ( 'NONE',  ( -1.966620079519992181, -21.27258529651320274, -1.500000000000002220 ) ) ;
#51742=DIRECTION ( 'NONE',  ( -3.773278334453080206E-23, 0.9999999999976377785, 2.173523156925979975E-06 ) ) ;
#51744=CARTESIAN_POINT ( 'NONE',  ( -91.16090919880674903, -25.31768024997816013, 4.634761245912265792 ) ) ;
#51745=FACE_OUTER_BOUND ( 'NONE', #72675, .T. ) ;
#51747=CARTESIAN_POINT ( 'NONE',  ( 19.67839991682829748, -11.23141783594569354, -1.500000000000002220 ) ) ;
#51749=CARTESIAN_POINT ( 'NONE',  ( -92.62287095715005592, -24.64898659630368627, 1.056161002820827921 ) ) ;
#51750=CARTESIAN_POINT ( 'NONE',  ( -99.55620429048340725, -23.47593901973091235, -1.443836447539001089 ) ) ;
#51751=CARTESIAN_POINT ( 'NONE',  ( 19.71268880909926580, -1.816447362451163450, 11.49999999999999645 ) ) ;
#51754=CARTESIAN_POINT ( 'NONE',  ( -119.5228709571500616, -24.66019654487200441, 8.947790411086108620 ) ) ;
#51755=ORIENTED_EDGE ( 'NONE', *, *, #72123, .T. ) ;
#51756=LINE ( 'NONE', #44639, #500 ) ;
#51757=CARTESIAN_POINT ( 'NONE',  ( -29.47844009783932862, -24.60094155636027580, 2.848996143664383141 ) ) ;
#51759=CARTESIAN_POINT ( 'NONE',  ( 10.18377579766961283, -19.05927572544859672, 11.49999999999998934 ) ) ;
#51761=CARTESIAN_POINT ( 'NONE',  ( -101.5562042904833930, -23.48786465467241413, 11.44779295918254469 ) ) ;
#51762=CARTESIAN_POINT ( 'NONE',  ( -109.5228709571500616, -23.47593901973090524, -1.443836447538996426 ) ) ;
#51764=CARTESIAN_POINT ( 'NONE',  ( -18.99895575154661742, -5.639348582513488140, -1.500000000000002220 ) ) ;
#51766=B_SPLINE_CURVE_WITH_KNOTS ( 'NONE', 3,
 ( #44324, #92465, #44820, #75740 ),
 .UNSPECIFIED., .F., .F.,
 ( 4, 4 ),
 ( 0.000000000000000000, 0.009506788565010804160 ),
 .UNSPECIFIED. ) ;
#51767=CARTESIAN_POINT ( 'NONE',  ( 0.8729654516333695824, -20.24016528753796962, 11.49999999999999645 ) ) ;
#51768=DIRECTION ( 'NONE',  ( 1.000000000000000000, 3.773278334444166432E-23, 8.201307841325785021E-29 ) ) ;
#51772=B_SPLINE_SURFACE_WITH_KNOTS ( 'NONE', 3, 3, ( 
 ( #14348, #31580, #133, #47318 ),
 ( #39190, #92971, #14848, #77237 ),
 ( #632, #77736, #32080, #85362 ),
 ( #70650, #38690, #70146, #92471 ),
 ( #69656, #63056, #39691, #45324 ),
 ( #15348, #76246, #99574, #6743 ),
 ( #53935, #45814, #23963, #54429 ) ),
 .UNSPECIFIED., .F., .F., .F.,
 ( 4, 3, 4 ),
 ( 4, 4 ),
 ( 0.7945040050992245861, 0.8970133687736505657, 0.9995227324480764342 ),
 ( 0.6196514592668809218, 0.6209502560550047567 ),
 .UNSPECIFIED. ) ;
#51773=CARTESIAN_POINT ( 'NONE',  ( -30.60464735295150263, -24.58764167366260622, 9.439037205594624780 ) ) ;
#51774=LINE ( 'NONE', #97441, #34728 ) ;
#51775=CARTESIAN_POINT ( 'NONE',  ( -71.52287095715010423, -23.96177878511308279, 10.65340807706330217 ) ) ;
#51777=CARTESIAN_POINT ( 'NONE',  ( -31.52287095715005449, -24.50321055353804311, 9.387540953477531147 ) ) ;
#51778=CARTESIAN_POINT ( 'NONE',  ( -5.826506878040391690, 19.21762618028343184, -1.500000000000002220 ) ) ;
#51780=ORIENTED_EDGE ( 'NONE', *, *, #77008, .T. ) ;
#51781=CARTESIAN_POINT ( 'NONE',  ( 20.53691900564983186, 10.01969956684014207, 11.49999999999999645 ) ) ;
#51782=CARTESIAN_POINT ( 'NONE',  ( -102.5228709571500616, -24.50216790748204332, 0.6166512839542633850 ) ) ;
#51783=CARTESIAN_POINT ( 'NONE',  ( -125.6228709571500559, -29.50250786944525672, 11.44777988621622633 ) ) ;
#51784=DIRECTION ( 'NONE',  ( -0.000000000000000000, 2.173523156925979552E-06, -0.9999999999976378895 ) ) ;
#51786=AXIS2_PLACEMENT_3D ( 'NONE', #83919, #74801, #14896 ) ;
#51787=EDGE_CURVE ( 'NONE', #47794, #58273, #89497, .T. ) ;
#51788=DIRECTION ( 'NONE',  ( 0.000000000000000000, 0.9999999999976377785, 2.173523156925979975E-06 ) ) ;
#51789=CARTESIAN_POINT ( 'NONE',  ( 4.981011153104904388, 21.88276397462241363, 11.49999999999999645 ) ) ;
#51790=EDGE_CURVE ( 'NONE', #33210, #5560, #1620, .T. ) ;
#51791=LINE ( 'NONE', #82725, #56610 ) ;
#51792=ORIENTED_EDGE ( 'NONE', *, *, #17255, .F. ) ;
#51794=CARTESIAN_POINT ( 'NONE',  ( -16.75749313124890350, -11.57646860041911019, -1.500000000000002220 ) ) ;
#51796=B_SPLINE_CURVE_WITH_KNOTS ( 'NONE', 3,
 ( #90189, #99288, #51636, #29786, #22154, #82571, #76443, #44014 ),
 .UNSPECIFIED., .F., .F.,
 ( 4, 2, 2, 4 ),
 ( 6.391158118959873630E-06, 0.002007136338672917044, 0.003007508928949899959, 0.004007881519226882440 ),
 .UNSPECIFIED. ) ;
#51797=CARTESIAN_POINT ( 'NONE',  ( 21.44032754495887261, 8.191337786432022483, -1.500000000000002220 ) ) ;
#51801=CARTESIAN_POINT ( 'NONE',  ( -37.62287095715006302, -24.33832256526968507, 0.1851278514119858165 ) ) ;
#51802=CARTESIAN_POINT ( 'NONE',  ( -77.59209893028688043, -24.15620529776628800, 10.23563542870659937 ) ) ;
#51803=VECTOR ( 'NONE', #27359, 1000.000000000000114 ) ;
#51805=CARTESIAN_POINT ( 'NONE',  ( 9.380127297304197143, -19.07726845333505494, 11.49999999999999645 ) ) ;
#51806=VERTEX_POINT ( 'NONE', #28596 ) ;
#51808=ORIENTED_EDGE ( 'NONE', *, *, #65552, .F. ) ;
#51809=CARTESIAN_POINT ( 'NONE',  ( -22.11311035156252558, 1.696007508605793301, 11.49999999999998934 ) ) ;
#51810=CARTESIAN_POINT ( 'NONE',  ( 19.39738937107077632, -6.937168198526852514, 11.49999999999998934 ) ) ;
#51811=B_SPLINE_CURVE_WITH_KNOTS ( 'NONE', 3,
 ( #43574, #11117, #10621, #81129, #74512, #20216 ),
 .UNSPECIFIED., .F., .F.,
 ( 4, 2, 4 ),
 ( 6.391158118959990520E-06, 0.001387004593080782460, 0.002767618028042605031 ),
 .UNSPECIFIED. ) ;
#51812=VECTOR ( 'NONE', #97133, 1000.000000000000114 ) ;
#51813=EDGE_LOOP ( 'NONE', ( #19097, #7228, #61426, #79283 ) ) ;
#51816=CARTESIAN_POINT ( 'NONE',  ( -121.6228709571500417, -24.65952944569305316, 1.056160979905705677 ) ) ;
#51817=ORIENTED_EDGE ( 'NONE', *, *, #44583, .T. ) ;
#51820=CARTESIAN_POINT ( 'NONE',  ( -127.4336594584713538, -25.30053190447140921, 4.607786779764230012 ) ) ;
#51821=CARTESIAN_POINT ( 'NONE',  ( -46.52287095715007581, -23.94994826722564696, -0.6494450866342706963 ) ) ;
#51822=CARTESIAN_POINT ( 'NONE',  ( -119.5895376238167245, -23.48783264082479150, -1.443836473390058384 ) ) ;
#51823=CARTESIAN_POINT ( 'NONE',  ( 12.91705851660734972, -16.24616318834520001, -1.500000000000002220 ) ) ;
#51824=CARTESIAN_POINT ( 'NONE',  ( -20.56741719582323213, 7.008553436993695485, 11.49999999999999645 ) ) ;
#51825=ORIENTED_EDGE ( 'NONE', *, *, #88413, .F. ) ;
#51826=CARTESIAN_POINT ( 'NONE',  ( -40.14671197708927508, -25.19036671141680017, 3.332572802394528910 ) ) ;
#51827=CARTESIAN_POINT ( 'NONE',  ( -41.62287095715006302, -29.50250786944525672, 11.44777988621624232 ) ) ;
#51828=CARTESIAN_POINT ( 'NONE',  ( -115.5222181705558882, -23.48783264082477018, -1.443836473390087916 ) ) ;
#51829=CARTESIAN_POINT ( 'NONE',  ( 1.585521478320181865, 22.38520322874704149, 11.49999999999998934 ) ) ;
#51830=CARTESIAN_POINT ( 'NONE',  ( -51.02503725990638372, -25.31296715355957616, 4.507473421736313490 ) ) ;
#51831=VERTEX_POINT ( 'NONE', #46194 ) ;
#51832=CARTESIAN_POINT ( 'NONE',  ( -59.52287095715005449, -23.95044443724991723, 10.65354141964649592 ) ) ;
#51833=CARTESIAN_POINT ( 'NONE',  ( -50.54482650861676518, -25.11141432701465703, 2.838324031928523894 ) ) ;
#51835=ORIENTED_EDGE ( 'NONE', *, *, #10579, .F. ) ;
#51836=CARTESIAN_POINT ( 'NONE',  ( -99.35333152103353882, -25.28669466114246944, 5.843841316355384841 ) ) ;
#51838=CARTESIAN_POINT ( 'NONE',  ( 18.63368790978032763, -10.32677859091227113, -1.500000000000002220 ) ) ;
#51841=CARTESIAN_POINT ( 'NONE',  ( 21.07893183998518438, -5.767110019903106455, 11.49999999999998934 ) ) ;
#51842=PLANE ( 'NONE',  #20594 ) ;
#51843=CARTESIAN_POINT ( 'NONE',  ( 22.16846167567618053, -4.910139430472912458, 11.49999999999998934 ) ) ;
#51845=CARTESIAN_POINT ( 'NONE',  ( -41.17181748269097596, -25.28892478857502368, 3.555109730339158336 ) ) ;
#51847=CARTESIAN_POINT ( 'NONE',  ( -21.91604229967229500, -0.6759211909499470705, -1.500000000000002220 ) ) ;
#51849=ORIENTED_EDGE ( 'NONE', *, *, #40103, .F. ) ;
#51850=CARTESIAN_POINT ( 'NONE',  ( -122.5900848267528289, -24.15620529776629510, 10.23563542870659582 ) ) ;
#51854=CARTESIAN_POINT ( 'NONE',  ( -116.6228709571499991, -24.33832256527049154, 0.1851278514138666176 ) ) ;
#51855=ADVANCED_FACE ( 'NONE', ( #39076 ), #23268, .T. ) ;
#51856=CARTESIAN_POINT ( 'NONE',  ( -39.62287095715004881, -23.48783264082477373, -1.443836473390072594 ) ) ;
#51857=CARTESIAN_POINT ( 'NONE',  ( -20.44305909758882933, -23.48154892321408482, 0.04347934593173589934 ) ) ;
#51858=CARTESIAN_POINT ( 'NONE',  ( -15.93125441714207646, -14.09135727244061265, -1.500000000000002220 ) ) ;
#51860=EDGE_CURVE ( 'NONE', #87031, #49847, #76704, .T. ) ;
#51863=CARTESIAN_POINT ( 'NONE',  ( -85.55841925135938197, -23.85016227208579664, -0.8807180028928368598 ) ) ;
#51864=CARTESIAN_POINT ( 'NONE',  ( -33.53809244281052315, -24.34968618360933235, 0.1864209137778845560 ) ) ;
#51865=CARTESIAN_POINT ( 'NONE',  ( -44.62287095715005592, -23.72773821059535848, 11.05748984161097503 ) ) ;
#51866=ORIENTED_EDGE ( 'NONE', *, *, #21085, .T. ) ;
#51867=CARTESIAN_POINT ( 'NONE',  ( -19.30006219055749739, -3.230038287793697283, 11.49999999999999645 ) ) ;
#51868=CARTESIAN_POINT ( 'NONE',  ( -58.62287095715002749, -23.96177878511307568, 10.65340807706330573 ) ) ;
#51871=EDGE_CURVE ( 'NONE', #87632, #88641, #70620, .T. ) ;
#51872=VERTEX_POINT ( 'NONE', #79137 ) ;
#51873=FACE_OUTER_BOUND ( 'NONE', #36082, .T. ) ;
#51874=CARTESIAN_POINT ( 'NONE',  ( -101.8264017983208021, -25.18997244373181843, 6.677177547450886763 ) ) ;
#51875=VECTOR ( 'NONE', #55353, 1000.000000000000114 ) ;
#51876=CARTESIAN_POINT ( 'NONE',  ( -122.5895376238167245, -23.47593901973091235, -1.443836447538997536 ) ) ;
#51877=CARTESIAN_POINT ( 'NONE',  ( -45.62287095715005592, -23.84047902841603062, -0.8780736468305723186 ) ) ;
#51878=CARTESIAN_POINT ( 'NONE',  ( -16.18664964019209052, -11.25563402961023662, 11.49999999999998934 ) ) ;
#51879=VECTOR ( 'NONE', #4930, 1000.000000000000114 ) ;
#51884=AXIS2_PLACEMENT_3D ( 'NONE', #39736, #41252, #1186 ) ;
#51889=CARTESIAN_POINT ( 'NONE',  ( -55.61923018639313199, -23.48783264082475952, -1.443836473390099462 ) ) ;
#51890=CARTESIAN_POINT ( 'NONE',  ( -63.52287095715004739, -23.47593901973090169, -1.443836447538996870 ) ) ;
#51892=B_SPLINE_CURVE_WITH_KNOTS ( 'NONE', 3,
 ( #88613, #3887, #40934, #65796 ),
 .UNSPECIFIED., .F., .F.,
 ( 4, 4 ),
 ( 0.000000000000000000, 9.999999999998206125E-05 ),
 .UNSPECIFIED. ) ;
#51893=CARTESIAN_POINT ( 'NONE',  ( -70.25652273905276957, -25.24515042782171648, 5.316157094516560377 ) ) ;
#51894=CARTESIAN_POINT ( 'NONE',  ( -71.52287095715006160, -23.47593901973090169, -1.443836447538996870 ) ) ;
#51895=CARTESIAN_POINT ( 'NONE',  ( -3.050325703546597822, 19.74810961616558913, 11.49999999999998934 ) ) ;
#51899=CARTESIAN_POINT ( 'NONE',  ( -63.52287095715006160, -24.33832256527048798, 0.1851278514138573750 ) ) ;
#51902=CARTESIAN_POINT ( 'NONE',  ( -66.52287095715007581, -23.96127896941631974, -0.6493128931038036900 ) ) ;
#51903=CARTESIAN_POINT ( 'NONE',  ( -66.62287095715005592, -24.65952944569304606, 1.056160979905696573 ) ) ;
#51905=CARTESIAN_POINT ( 'NONE',  ( -39.52202227182803540, -23.48783264082476308, -1.443836473390098352 ) ) ;
#51906=EDGE_CURVE ( 'NONE', #30329, #63299, #49217, .T. ) ;
#51907=CARTESIAN_POINT ( 'NONE',  ( -28.41293738586069040, -25.26026315677608380, 1.764151969445674428 ) ) ;
#51908=CARTESIAN_POINT ( 'NONE',  ( -51.04357394935764347, -25.31574462869783204, 4.940877928535408969 ) ) ;
#51909=ORIENTED_EDGE ( 'NONE', *, *, #64051, .F. ) ;
#51911=CARTESIAN_POINT ( 'NONE',  ( -127.5217006469362673, -23.96119346886880663, -0.6495511937832001426 ) ) ;
#51913=CARTESIAN_POINT ( 'NONE',  ( -20.21730713243277933, 1.494317884549376974, -1.500000000000002220 ) ) ;
#51915=CARTESIAN_POINT ( 'NONE',  ( -98.89303308397306580, -25.26498937201382233, 6.110950154240443410 ) ) ;
#51918=CARTESIAN_POINT ( 'NONE',  ( -77.52287095715007581, -23.72773821059536914, 11.05748984161097326 ) ) ;
#51919=CARTESIAN_POINT ( 'NONE',  ( -46.52287095715005449, -24.50321055353803956, 9.387540953477520489 ) ) ;
#51920=CARTESIAN_POINT ( 'NONE',  ( -9.072532997253766496, -17.89392090870456542, -1.500000000000002220 ) ) ;
#51921=CARTESIAN_POINT ( 'NONE',  ( 8.398332666215036824, -19.25654272332048578, 11.49999999999999645 ) ) ;
#51922=CARTESIAN_POINT ( 'NONE',  ( -28.60093854151381265, -24.95576419111307231, 7.235735347421135444 ) ) ;
#51924=CARTESIAN_POINT ( 'NONE',  ( -22.07534667767119174, -0.2742745133902674826, 11.49999999999998934 ) ) ;
#51926=CARTESIAN_POINT ( 'NONE',  ( 19.18951349294833264, 7.196795126939715459, -1.500000000000002220 ) ) ;
#51927=CARTESIAN_POINT ( 'NONE',  ( -93.58953762381673869, -23.47596703998600631, 11.44779298504227683 ) ) ;
#51932=CARTESIAN_POINT ( 'NONE',  ( -31.63564585891770520, -24.34968618360933590, 0.1864209137778850556 ) ) ;
#51933=ORIENTED_EDGE ( 'NONE', *, *, #47565, .F. ) ;
#51935=CARTESIAN_POINT ( 'NONE',  ( -55.52287095715005449, -23.48783264082477018, -1.443836473390094577 ) ) ;
#51936=CARTESIAN_POINT ( 'NONE',  ( -100.4498239493576648, -25.04307398257883932, 7.563174194274490780 ) ) ;
#51937=CARTESIAN_POINT ( 'NONE',  ( -76.54602688947991851, -24.34968618360934300, 0.1864209137778858327 ) ) ;
#51938=CARTESIAN_POINT ( 'NONE',  ( -13.12974562303265813, -15.89414520977026513, -1.500000000000002220 ) ) ;
#51939=CARTESIAN_POINT ( 'NONE',  ( -14.38888013576714719, -16.06800976983558726, 11.49999999999999645 ) ) ;
#51940=EDGE_LOOP ( 'NONE', ( #94243, #87853, #5019, #70084, #9129 ) ) ;
#51941=CARTESIAN_POINT ( 'NONE',  ( -35.52287095715005449, -23.48783264083451883, -1.443836473374936258 ) ) ;
#51943=CARTESIAN_POINT ( 'NONE',  ( 20.54922051473491607, -8.805037660420627077, -1.500000000000002220 ) ) ;
#51945=CARTESIAN_POINT ( 'NONE',  ( -84.51017505570197841, -24.15543982623907482, -0.2315651400026630391 ) ) ;
#51947=LINE ( 'NONE', #90007, #3138 ) ;
#51950=B_SPLINE_CURVE_WITH_KNOTS ( 'NONE', 3,
 ( #87602, #39423, #18084, #31813 ),
 .UNSPECIFIED., .F., .F.,
 ( 4, 4 ),
 ( 0.000000000000000000, 1.000000000000000000 ),
 .UNSPECIFIED. ) ;
#51952=CARTESIAN_POINT ( 'NONE',  ( -11.44352472427880052, 17.46665840655709090, 11.49999999999998934 ) ) ;
#51954=CARTESIAN_POINT ( 'NONE',  ( -67.58777801654929362, -24.35071581493543746, 9.817618358456023486 ) ) ;
#51958=CARTESIAN_POINT ( 'NONE',  ( -100.6412043750470104, -23.48786465467241413, 11.44779295918254469 ) ) ;
#51959=CARTESIAN_POINT ( 'NONE',  ( 19.82261944725993175, 7.364942908566579405, -1.500000000000002220 ) ) ;
#51960=ORIENTED_EDGE ( 'NONE', *, *, #94921, .T. ) ;
#51962=CARTESIAN_POINT ( 'NONE',  ( -48.87558633688828991, -25.25869780337663784, 6.071246232422383926 ) ) ;
#51963=CARTESIAN_POINT ( 'NONE',  ( -48.62287095715004881, -24.66019654487199020, 8.947790411086135265 ) ) ;
#51965=CARTESIAN_POINT ( 'NONE',  ( -38.52287095715006870, -23.48786465467241058, 11.44779295918255180 ) ) ;
#51966=CARTESIAN_POINT ( 'NONE',  ( 5.219777686717518961, -21.12652377152128480, -1.500000000000002220 ) ) ;
#51967=CARTESIAN_POINT ( 'NONE',  ( -31.24388727629347784, -24.87479601683088148, 8.247789944647559324 ) ) ;
#51968=EDGE_CURVE ( 'NONE', #61101, #45280, #60926, .T. ) ;
#51969=CARTESIAN_POINT ( 'NONE',  ( -1.228339276683141579, -22.28195500894762660, 11.49999999999999645 ) ) ;
#51971=FACE_OUTER_BOUND ( 'NONE', #33755, .T. ) ;
#51975=ORIENTED_EDGE ( 'NONE', *, *, #68857, .T. ) ;
#51976=VERTEX_POINT ( 'NONE', #41598 ) ;
#51977=EDGE_CURVE ( 'NONE', #14722, #36363, #47703, .T. ) ;
#51979=CARTESIAN_POINT ( 'NONE',  ( -127.9228709571500531, -23.47593901973090524, -1.443836447538996204 ) ) ;
#51980=EDGE_CURVE ( 'NONE', #84981, #60030, #49716, .T. ) ;
#51982=CARTESIAN_POINT ( 'NONE',  ( -49.57059674196057841, -25.31466356504994053, 4.840235729264941611 ) ) ;
#51983=CARTESIAN_POINT ( 'NONE',  ( -5.843762028675351772, -18.45606589188993141, -1.500000000000002220 ) ) ;
#51984=CARTESIAN_POINT ( 'NONE',  ( -36.55620429048340014, -24.66019654487199020, 8.947790411086138818 ) ) ;
#51985=EDGE_LOOP ( 'NONE', ( #1022, #96961, #56563, #24139 ) ) ;
#51986=CARTESIAN_POINT ( 'NONE',  ( 18.67713048845720181, -5.233370074711279685, 11.49999999999999645 ) ) ;
#51987=CARTESIAN_POINT ( 'NONE',  ( -30.47287095715007510, -23.47594215783195537, -5.102550391006585557E-05 ) ) ;
#51988=EDGE_CURVE ( 'NONE', #39987, #29613, #93862, .T. ) ;
#51989=ORIENTED_EDGE ( 'NONE', *, *, #92176, .F. ) ;
#51991=CARTESIAN_POINT ( 'NONE',  ( -29.52287095715006160, -29.50250243563707286, 8.947779751028683393 ) ) ;
#51993=CARTESIAN_POINT ( 'NONE',  ( -63.93899109588087271, -24.04668586515358797, 10.47594215909545312 ) ) ;
#51994=CARTESIAN_POINT ( 'NONE',  ( 2.166912399371504705, 19.51343182558466793, 11.49999999999998934 ) ) ;
#51996=VERTEX_POINT ( 'NONE', #78620 ) ;
#51997=CARTESIAN_POINT ( 'NONE',  ( -21.33164055427280914, -3.227942221655450972, -1.500000000000002220 ) ) ;
#51998=CARTESIAN_POINT ( 'NONE',  ( -33.47773199953535084, -24.66019654487198665, 8.947790411086133489 ) ) ;
#51999=CARTESIAN_POINT ( 'NONE',  ( -70.35718658181241381, -25.25639601273455526, 7.100646501951180412 ) ) ;
#52001=B_SPLINE_CURVE_WITH_KNOTS ( 'NONE', 3,
 ( #19442, #72248, #2740, #41806 ),
 .UNSPECIFIED., .F., .F.,
 ( 4, 4 ),
 ( 0.06983579250763341517, 0.07884222377974890728 ),
 .UNSPECIFIED. ) ;
#52003=CARTESIAN_POINT ( 'NONE',  ( -72.62287095715005592, -29.50250243563736774, 8.947779886222143375 ) ) ;
#52004=CARTESIAN_POINT ( 'NONE',  ( 18.09022303007301247, 14.20294132079179938, -1.500000000000002220 ) ) ;
#52007=CARTESIAN_POINT ( 'NONE',  ( -50.09975158262200523, -25.30285855287542773, 4.744951912546983230 ) ) ;
#52008=CARTESIAN_POINT ( 'NONE',  ( -11.28321777122536140, 16.66956161807075887, 11.49999999999999645 ) ) ;
#52009=CARTESIAN_POINT ( 'NONE',  ( -109.3293036055952143, -25.28814155227650318, 3.229614981432298304 ) ) ;
#52014=EDGE_CURVE ( 'NONE', #66289, #38454, #81598, .T. ) ;
#52015=CARTESIAN_POINT ( 'NONE',  ( 13.99221305778824487, -14.08248706038611964, 11.49999999999998934 ) ) ;
#52016=CARTESIAN_POINT ( 'NONE',  ( -113.5569085991196090, -23.73766607897670866, -1.055555164236448240 ) ) ;
#52017=CARTESIAN_POINT ( 'NONE',  ( 1.028332004353105233, 19.75660188889424518, -1.500000000000002220 ) ) ;
#52018=CARTESIAN_POINT ( 'NONE',  ( -126.5547688801620438, -24.66019654487200796, 8.947790411086103290 ) ) ;
#52019=ADVANCED_FACE ( 'NONE', ( #24355 ), #70533, .T. ) ;
#52024=CARTESIAN_POINT ( 'NONE',  ( 18.07348078632662691, -10.09602009226539288, 11.49999999999999645 ) ) ;
#52027=CARTESIAN_POINT ( 'NONE',  ( -50.15966858932511485, -25.25138676263039983, 5.214258431718429065 ) ) ;
#52028=CARTESIAN_POINT ( 'NONE',  ( 11.07647423179810531, -19.82844882884714366, 11.49999999999999645 ) ) ;
#52029=EDGE_CURVE ( 'NONE', #10158, #76180, #41710, .T. ) ;
#52031=CARTESIAN_POINT ( 'NONE',  ( -78.52287095715006160, -24.65952944569304606, 1.056160979905698794 ) ) ;
#52032=CARTESIAN_POINT ( 'NONE',  ( -33.55620429048339304, -24.66019654487199020, 8.947790411086137041 ) ) ;
#52038=CARTESIAN_POINT ( 'NONE',  ( -100.3036073397659322, -25.12344534561801268, 7.099021671109709608 ) ) ;
#52039=CARTESIAN_POINT ( 'NONE',  ( 17.53461989915211916, -14.66684187699354425, -1.500000000000002220 ) ) ;
#52040=CARTESIAN_POINT ( 'NONE',  ( -29.62954789768681962, -24.43759654968573614, 0.6176547996449982536 ) ) ;
#52041=CARTESIAN_POINT ( 'NONE',  ( 13.05104812959431548, -17.15854754814989391, -1.500000000000002220 ) ) ;
#52043=CARTESIAN_POINT ( 'NONE',  ( -115.5562042904833930, -24.99156044556202616, 7.747789690856173195 ) ) ;
#52044=CARTESIAN_POINT ( 'NONE',  ( -16.99934442671578694, -14.85117937636706031, 11.49999999999999645 ) ) ;
#52045=EDGE_LOOP ( 'NONE', ( #32922, #51849, #71298, #4681 ) ) ;
#52046=CARTESIAN_POINT ( 'NONE',  ( -70.00627666057835086, -25.24754250677208134, 4.873906482351993752 ) ) ;
#52047=CARTESIAN_POINT ( 'NONE',  ( 16.65356921002588919, 14.36988287374134821, -1.500000000000002220 ) ) ;
#52048=EDGE_CURVE ( 'NONE', #5456, #12501, #13819, .T. ) ;
#52049=CARTESIAN_POINT ( 'NONE',  ( -105.6293760709154128, -24.40133493613049964, 9.663955038902797057 ) ) ;
#52050=CARTESIAN_POINT ( 'NONE',  ( -28.88518304243395818, -25.21724837498792127, 6.883446113543877587 ) ) ;
#52051=VERTEX_POINT ( 'NONE', #87764 ) ;
#52053=CARTESIAN_POINT ( 'NONE',  ( -116.6228709571500559, -29.50250243563736774, 8.947779886222134493 ) ) ;
#52054=B_SPLINE_CURVE_WITH_KNOTS ( 'NONE', 3,
 ( #100387, #9065, #16174, #48144 ),
 .UNSPECIFIED., .F., .F.,
 ( 4, 4 ),
 ( 0.8193651591418213975, 0.8203659061825868681 ),
 .UNSPECIFIED. ) ;
#52055=ORIENTED_EDGE ( 'NONE', *, *, #97587, .T. ) ;
#52056=CARTESIAN_POINT ( 'NONE',  ( -116.5228709571500616, -24.65952944569305316, 1.056160979905705899 ) ) ;
#52057=EDGE_CURVE ( 'NONE', #30457, #83907, #75459, .T. ) ;
#52058=VERTEX_POINT ( 'NONE', #63444 ) ;
#52062=CARTESIAN_POINT ( 'NONE',  ( -71.92287095715006728, -23.47596703998600631, 11.44779298504227860 ) ) ;
#52063=CARTESIAN_POINT ( 'NONE',  ( -57.54804246586016347, -24.15543982623907127, -0.2315651400026663420 ) ) ;
#52064=CARTESIAN_POINT ( 'NONE',  ( -8.052747710315523832, 18.77774781879659116, -1.500000000000002220 ) ) ;
#52067=ADVANCED_FACE ( 'NONE', ( #33465 ), #26361, .T. ) ;
#52068=CARTESIAN_POINT ( 'NONE',  ( -30.59167141582165428, -24.92410949913932683, 1.600845668900849672 ) ) ;
#52069=EDGE_CURVE ( 'NONE', #76858, #95755, #83917, .T. ) ;
#52070=CARTESIAN_POINT ( 'NONE',  ( -54.52287095715005449, -23.48783264082476308, -1.443836473390096797 ) ) ;
#52072=ORIENTED_EDGE ( 'NONE', *, *, #39530, .T. ) ;
#52073=CARTESIAN_POINT ( 'NONE',  ( -49.62287095715004170, -23.47596703998600631, 11.44779298504227505 ) ) ;
#52074=CARTESIAN_POINT ( 'NONE',  ( -102.6228709571500559, -29.50247984919015209, -1.443849546365050029 ) ) ;
#52076=CARTESIAN_POINT ( 'NONE',  ( 11.01739540223112357, 17.63107602209319680, 11.49999999999998934 ) ) ;
#52077=AXIS2_PLACEMENT_3D ( 'NONE', #76302, #29643, #91538 ) ;
#52078=VERTEX_POINT ( 'NONE', #80648 ) ;
#52079=DIRECTION ( 'NONE',  ( -3.773278334444166432E-23, 1.000000000000000000, 0.000000000000000000 ) ) ;
#52080=EDGE_LOOP ( 'NONE', ( #39293, #27120, #52379, #16333 ) ) ;
#52081=DIRECTION ( 'NONE',  ( -3.773278334453079030E-23, 0.9999999999976377785, 2.173523156925979128E-06 ) ) ;
#52082=VERTEX_POINT ( 'NONE', #88769 ) ;
#52084=DIRECTION ( 'NONE',  ( -3.773278334444167608E-23, 1.000000000000000000, 0.000000000000000000 ) ) ;
#52085=CARTESIAN_POINT ( 'NONE',  ( -76.52287095715011844, -23.95044443724992789, 10.65354141964649415 ) ) ;
#52086=CARTESIAN_POINT ( 'NONE',  ( -60.55620429048339304, -23.48786465467241058, 11.44779295918254824 ) ) ;
#52089=CARTESIAN_POINT ( 'NONE',  ( -20.57447749561850969, 8.151157241358404804, 11.49999999999999645 ) ) ;
#52092=CARTESIAN_POINT ( 'NONE',  ( 20.48348528492645571, -9.684159049092739835, -1.500000000000002220 ) ) ;
#52093=FACE_OUTER_BOUND ( 'NONE', #63738, .T. ) ;
#52094=EDGE_LOOP ( 'NONE', ( #54433, #73434, #18021, #71607 ) ) ;
#52095=AXIS2_PLACEMENT_3D ( 'NONE', #10690, #64004, #41651 ) ;
#52096=EDGE_LOOP ( 'NONE', ( #22825, #78650, #88621, #80376, #78277, #32812, #9275, #4031, #83180, #8905, #4059, #55448 ) ) ;
#52098=DIRECTION ( 'NONE',  ( 0.000000000000000000, 0.9999999999976377785, 2.173523156925979975E-06 ) ) ;
#52099=B_SPLINE_CURVE_WITH_KNOTS ( 'NONE', 3,
 ( #17877, #80274, #10769, #88898 ),
 .UNSPECIFIED., .F., .F.,
 ( 4, 4 ),
 ( 0.000000000000000000, 9.999999999998897304E-05 ),
 .UNSPECIFIED. ) ;
#52100=B_SPLINE_CURVE_WITH_KNOTS ( 'NONE', 3,
 ( #74692, #28033, #81817, #59990 ),
 .UNSPECIFIED., .F., .F.,
 ( 4, 4 ),
 ( 0.000000000000000000, 9.999999999998900014E-05 ),
 .UNSPECIFIED. ) ;
#52102=CARTESIAN_POINT ( 'NONE',  ( -17.50950832565593984, 9.922426906265528146, 11.49999999999998934 ) ) ;
#52105=ORIENTED_EDGE ( 'NONE', *, *, #64730, .F. ) ;
#52107=CARTESIAN_POINT ( 'NONE',  ( -12.31279356157217109, -18.55646752483835016, -1.500000000000002220 ) ) ;
#52111=CARTESIAN_POINT ( 'NONE',  ( -89.62287095715005592, -23.72773821059535848, 11.05748984161097681 ) ) ;
#52112=CARTESIAN_POINT ( 'NONE',  ( -26.80500567364604336, -24.59566541176759813, 1.842733277147198923 ) ) ;
#52117=CARTESIAN_POINT ( 'NONE',  ( -11.52932745282126703, -15.74164922852205173, -1.500000000000002220 ) ) ;
#52118=CARTESIAN_POINT ( 'NONE',  ( -15.31780299886000485, -15.04297462106122474, -1.500000000000002220 ) ) ;
#52120=CARTESIAN_POINT ( 'NONE',  ( -46.55620429048339304, -23.47596703998600276, 11.44779298504227505 ) ) ;
#52122=CARTESIAN_POINT ( 'NONE',  ( -22.75767140345847750, 1.815691853630000629, -1.500000000000002220 ) ) ;
#52125=FACE_OUTER_BOUND ( 'NONE', #38016, .T. ) ;
#52127=CARTESIAN_POINT ( 'NONE',  ( 18.82558416981596139, 6.732768832687442639, 11.49999999999999645 ) ) ;
#52128=CARTESIAN_POINT ( 'NONE',  ( -50.52287095715005449, -24.63287334234177450, 0.9662140553045359681 ) ) ;
#52129=CARTESIAN_POINT ( 'NONE',  ( -57.58953762381671737, -24.64898659630367916, 1.056161002820383610 ) ) ;
#52132=DIRECTION ( 'NONE',  ( -1.000000000000000000, -3.773278334444167608E-23, -8.201307833595939069E-29 ) ) ;
#52133=DIRECTION ( 'NONE',  ( 3.773278334444167608E-23, -1.000000000000000000, 0.000000000000000000 ) ) ;
#52134=CARTESIAN_POINT ( 'NONE',  ( -21.62197530259306788, 2.132803791230205359, -1.500000000000002220 ) ) ;
#52136=CARTESIAN_POINT ( 'NONE',  ( -7.889300446747370188, -17.95381117360125955, -1.500000000000002220 ) ) ;
#52137=CARTESIAN_POINT ( 'NONE',  ( -100.1650658605970392, -25.13691562650546985, 7.079980769990460665 ) ) ;
#52138=EDGE_LOOP ( 'NONE', ( #4793, #75229, #86647, #87142 ) ) ;
#52140=DIRECTION ( 'NONE',  ( 1.000000000000000000, 3.773278334444167608E-23, 8.201307833595939069E-29 ) ) ;
#52141=CARTESIAN_POINT ( 'NONE',  ( -123.9228709571500531, -23.47596703998600631, 11.44779298504228038 ) ) ;
#52142=CARTESIAN_POINT ( 'NONE',  ( -0.3173379506236611580, 20.48240526196808631, 11.49999999999999645 ) ) ;
#52144=VECTOR ( 'NONE', #39395, 1000.000000000000114 ) ;
#52145=CARTESIAN_POINT ( 'NONE',  ( -113.5228709571501327, -24.66019654487200441, 8.947790411086112172 ) ) ;
#52146=ORIENTED_EDGE ( 'NONE', *, *, #21678, .T. ) ;
#52148=CARTESIAN_POINT ( 'NONE',  ( -40.35585260198725877, -25.28892422734320178, 3.296896784922714652 ) ) ;
#52149=DIRECTION ( 'NONE',  ( 0.000000000000000000, -2.173523156925980399E-06, 0.9999999999976378895 ) ) ;
#52150=CARTESIAN_POINT ( 'NONE',  ( -123.5228709571500474, -23.47593901973090524, -1.443836447538996204 ) ) ;
#52153=AXIS2_PLACEMENT_3D ( 'NONE', #970, #68978, #53770 ) ;
#52154=CARTESIAN_POINT ( 'NONE',  ( 1.550618966079767347, 22.99078241098900932, 11.49999999999999645 ) ) ;
#52155=CARTESIAN_POINT ( 'NONE',  ( -15.20078144808659992, 16.97451310947862169, 11.49999999999998934 ) ) ;
#52156=DIRECTION ( 'NONE',  ( -3.773278334453079030E-23, 0.9999999999976377785, 2.173523156925979128E-06 ) ) ;
#52158=CARTESIAN_POINT ( 'NONE',  ( -49.51604314152774577, -25.26360598679406166, 3.877879557975262070 ) ) ;
#52160=CARTESIAN_POINT ( 'NONE',  ( -106.5228709571500758, -29.50247984919015209, -1.443849546365048253 ) ) ;
#52161=FACE_OUTER_BOUND ( 'NONE', #4667, .T. ) ;
#52162=CARTESIAN_POINT ( 'NONE',  ( 19.94191871449930531, -9.063712221575384476, 11.49999999999998934 ) ) ;
#52165=CARTESIAN_POINT ( 'NONE',  ( -87.51796210385577979, -23.73791477778911840, 11.05961554403170588 ) ) ;
#52166=FACE_OUTER_BOUND ( 'NONE', #71949, .T. ) ;
#52167=LINE ( 'NONE', #44053, #78403 ) ;
#52168=CARTESIAN_POINT ( 'NONE',  ( -112.6228709571501270, -23.94994826722516379, -0.6494450866351680896 ) ) ;
#52171=CARTESIAN_POINT ( 'NONE',  ( 19.09590870110849181, 7.302211495713927469, -1.500000000000002220 ) ) ;
#52174=ORIENTED_EDGE ( 'NONE', *, *, #6221, .T. ) ;
#52176=CARTESIAN_POINT ( 'NONE',  ( 1.550618966079767347, 22.99078241098900932, 11.49999999999998934 ) ) ;
#52177=CARTESIAN_POINT ( 'NONE',  ( -61.64237931368420220, -23.96119346886880308, -0.6495511937832122440 ) ) ;
#52179=CARTESIAN_POINT ( 'NONE',  ( -17.47620107869530770, 10.18187089365592612, -1.500000000000002220 ) ) ;
#52180=ORIENTED_EDGE ( 'NONE', *, *, #12419, .F. ) ;
#52181=EDGE_CURVE ( 'NONE', #92642, #61188, #34329, .T. ) ;
#52182=CARTESIAN_POINT ( 'NONE',  ( -48.52287095715005449, -24.33927499327854349, 9.819080762295810061 ) ) ;
#52183=ADVANCED_FACE ( 'NONE', ( #4030 ), #35480, .T. ) ;
#52184=CARTESIAN_POINT ( 'NONE',  ( -41.52762579262719100, -25.31532796546315822, 5.102889718565096544 ) ) ;
#52186=CARTESIAN_POINT ( 'NONE',  ( -101.5228709571501184, -24.51387760970725793, 9.387446482453407626 ) ) ;
#52187=CARTESIAN_POINT ( 'NONE',  ( -125.6228709571500559, -29.50249982740957577, 7.747779886224967605 ) ) ;
#52188=CARTESIAN_POINT ( 'NONE',  ( 6.029407872858970840, -20.54391778677962677, 11.49999999999999645 ) ) ;
#52191=EDGE_CURVE ( 'NONE', #4006, #2140, #535, .T. ) ;
#52192=ORIENTED_EDGE ( 'NONE', *, *, #90091, .F. ) ;
#52193=B_SPLINE_CURVE_WITH_KNOTS ( 'NONE', 3,
 ( #29856, #75019, #97860, #53210 ),
 .UNSPECIFIED., .F., .F.,
 ( 4, 4 ),
 ( 0.000000000000000000, 9.999999999998897304E-05 ),
 .UNSPECIFIED. ) ;
#52194=CARTESIAN_POINT ( 'NONE',  ( -20.39401028033356766, -3.670942005906183692, -1.500000000000002220 ) ) ;
#52197=B_SPLINE_SURFACE_WITH_KNOTS ( 'NONE', 3, 3, ( 
 ( #24039, #15427, #94055, #94554 ),
 ( #54013, #46388, #55512, #85950 ),
 ( #23527, #78321, #8827, #69733 ),
 ( #1221, #86447, #16932, #78816 ),
 ( #54505, #47897, #9312, #40277 ),
 ( #1720, #63635, #32657, #58019 ),
 ( #87448, #17940, #65639, #96066 ) ),
 .UNSPECIFIED., .F., .F., .F.,
 ( 4, 3, 4 ),
 ( 4, 4 ),
 ( 0.7945040050992232539, 0.8970133687736493444, 0.9995227324480754350 ),
 ( 0.1595345371825157288, 0.1606209134664254301 ),
 .UNSPECIFIED. ) ;
#52198=CARTESIAN_POINT ( 'NONE',  ( -123.6228709571500559, -23.48786465467241769, 11.44779295918253759 ) ) ;
#52202=CARTESIAN_POINT ( 'NONE',  ( 11.23609023086081038, -17.74952302366565604, -1.500000000000002220 ) ) ;
#52203=EDGE_CURVE ( 'NONE', #17176, #37373, #16167, .T. ) ;
#52204=CARTESIAN_POINT ( 'NONE',  ( -6.321128248299066499, 21.05883132939252533, 11.49999999999999645 ) ) ;
#52205=CARTESIAN_POINT ( 'NONE',  ( -37.60902819999402880, -23.73791477778911485, 11.05961554403171121 ) ) ;
#52206=CARTESIAN_POINT ( 'NONE',  ( -14.39138815452349718, -17.32352244779961481, -1.500000000000002220 ) ) ;
#52207=CARTESIAN_POINT ( 'NONE',  ( 8.737904895026865404, 19.08465823478955414, -1.500000000000002220 ) ) ;
#52208=CARTESIAN_POINT ( 'NONE',  ( -80.62287095715005592, -24.99132157543084531, 2.256160258750667502 ) ) ;
#52209=CARTESIAN_POINT ( 'NONE',  ( -119.5893875598164158, -24.35071581493544457, 9.817618358456018157 ) ) ;
#52211=ORIENTED_EDGE ( 'NONE', *, *, #70090, .F. ) ;
#52215=B_SPLINE_CURVE_WITH_KNOTS ( 'NONE', 3,
 ( #61435, #53319, #51820, #76131, #29964, #84752, #76625, #83749, #92362, #37080, #22335, #14229, #6127, #60933, #82749, #52316, #44702, #75138 ),
 .UNSPECIFIED., .F., .F.,
 ( 4, 2, 2, 2, 2, 2, 2, 2, 4 ),
 ( 1.734723475976807094E-18, 0.0005889166363242025149, 0.001177833272648403295, 0.001766749908972604184, 0.002355666545296804856, 0.002944583181621005744, 0.003533499817945206633, 0.004122416454269406220, 0.004711333090593606242 ),
 .UNSPECIFIED. ) ;
#52217=AXIS2_PLACEMENT_3D ( 'NONE', #40666, #42678, #95943 ) ;
#52219=EDGE_CURVE ( 'NONE', #70136, #52051, #57352, .T. ) ;
#52220=CARTESIAN_POINT ( 'NONE',  ( 2.695732861974529104, -21.29187259674557708, -1.500000000000002220 ) ) ;
#52221=CARTESIAN_POINT ( 'NONE',  ( -86.62287095715004170, -23.73934037231756733, 11.05740245334328975 ) ) ;
#52222=EDGE_LOOP ( 'NONE', ( #56823, #64969, #10935, #13871 ) ) ;
#52223=CARTESIAN_POINT ( 'NONE',  ( -19.14942259116913092, -8.910193081567555851, 11.49999999999998934 ) ) ;
#52224=CARTESIAN_POINT ( 'NONE',  ( -60.62287095715004881, -25.00182538069145011, 7.747789668545098429 ) ) ;
#52225=CARTESIAN_POINT ( 'NONE',  ( -64.63657109733628658, -24.15543982623906771, -0.2315651400026674800 ) ) ;
#52226=CARTESIAN_POINT ( 'NONE',  ( -64.62287095715005592, -23.48783264082478084, -1.443836473390069042 ) ) ;
#52229=CARTESIAN_POINT ( 'NONE',  ( -20.57447749561850969, 8.151157241358404804, -1.500000000000002220 ) ) ;
#52230=CARTESIAN_POINT ( 'NONE',  ( -116.6235093916941992, -24.65952944569305316, 1.056160979905712560 ) ) ;
#52233=DIRECTION ( 'NONE',  ( 0.000000000000000000, 2.173523156925980399E-06, -0.9999999999976378895 ) ) ;
#52236=CARTESIAN_POINT ( 'NONE',  ( -100.5114892534503639, -24.40034930558991633, 0.3402023900116076804 ) ) ;
#52238=CARTESIAN_POINT ( 'NONE',  ( 6.036767712469883307, 18.47306877840545170, 11.49999999999998934 ) ) ;
#52240=CARTESIAN_POINT ( 'NONE',  ( 18.17913347391500523, 11.28257676469832660, 11.49999999999998934 ) ) ;
#52241=CARTESIAN_POINT ( 'NONE',  ( -113.5895376238167245, -23.48786465467241769, 11.44779295918254114 ) ) ;
#52242=DIRECTION ( 'NONE',  ( -3.773278334453079618E-23, 0.9999999999976377785, 2.173523156925979975E-06 ) ) ;
#52243=ADVANCED_FACE ( 'NONE', ( #72435 ), #40978, .T. ) ;
#52244=CARTESIAN_POINT ( 'NONE',  ( -106.5228709571500758, -24.65952944569305316, 1.056160979905704123 ) ) ;
#52245=LINE ( 'NONE', #7057, #71724 ) ;
#52246=CARTESIAN_POINT ( 'NONE',  ( -21.16596634977960179, 8.012090315382277339, -1.500000000000002220 ) ) ;
#52247=VERTEX_POINT ( 'NONE', #48096 ) ;
#52248=LINE ( 'NONE', #68469, #15792 ) ;
#52250=CARTESIAN_POINT ( 'NONE',  ( -18.77405512783484198, 6.205181830411797606, 11.49999999999999645 ) ) ;
#52251=CARTESIAN_POINT ( 'NONE',  ( -59.62287095715004170, -24.65952944569304606, 1.056160979905694131 ) ) ;
#52253=CARTESIAN_POINT ( 'NONE',  ( -119.6228709571500417, -24.66019654487199730, 8.947790411086121054 ) ) ;
#52254=ORIENTED_EDGE ( 'NONE', *, *, #36459, .F. ) ;
#52257=CARTESIAN_POINT ( 'NONE',  ( 17.85095790706337127, 12.24325521369631176, -1.500000000000002220 ) ) ;
#52259=CARTESIAN_POINT ( 'NONE',  ( -70.52287095715007581, -25.00158670708909625, 2.256160236439166411 ) ) ;
#52261=CARTESIAN_POINT ( 'NONE',  ( -40.52287095715005449, -24.99156044556202261, 7.747789690856173195 ) ) ;
#52262=CARTESIAN_POINT ( 'NONE',  ( -19.78623529325263775, -1.157695164950638844, 11.49999999999998934 ) ) ;
#52263=ORIENTED_EDGE ( 'NONE', *, *, #56281, .T. ) ;
#52264=CARTESIAN_POINT ( 'NONE',  ( 8.194921280291850962, -18.63391395107102610, 11.49999999999999645 ) ) ;
#52268=ORIENTED_EDGE ( 'NONE', *, *, #77071, .F. ) ;
#52269=CARTESIAN_POINT ( 'NONE',  ( -30.56674980027052158, -25.57033040079278052, 6.142048374048878046 ) ) ;
#52271=CARTESIAN_POINT ( 'NONE',  ( -99.55620429048340725, -23.48786465467241769, 11.44779295918254114 ) ) ;
#52272=LINE ( 'NONE', #35556, #73222 ) ;
#52273=CARTESIAN_POINT ( 'NONE',  ( -87.52287095715006160, -23.47596703998600631, 11.44779298504228393 ) ) ;
#52274=CARTESIAN_POINT ( 'NONE',  ( -9.072532997253766496, -17.89392090870456542, -1.500000000000002220 ) ) ;
#52278=CARTESIAN_POINT ( 'NONE',  ( 19.59772090806136902, -11.66877021596143926, 11.49999999999999645 ) ) ;
#52279=CARTESIAN_POINT ( 'NONE',  ( -30.47287095715009286, -25.14093768624189451, 3.040070784493352551 ) ) ;
#52281=CARTESIAN_POINT ( 'NONE',  ( -86.62287095715004170, -23.72747288104441665, -1.053458166803661555 ) ) ;
#52282=CARTESIAN_POINT ( 'NONE',  ( -67.62287095715005592, -23.48783264082478794, -1.443836473390067265 ) ) ;
#52284=B_SPLINE_CURVE_WITH_KNOTS ( 'NONE', 3,
 ( #31634, #52996, #22508, #8304 ),
 .UNSPECIFIED., .F., .F.,
 ( 4, 4 ),
 ( 0.000000000000000000, 1.000000000000000000 ),
 .UNSPECIFIED. ) ;
#52285=CARTESIAN_POINT ( 'NONE',  ( -31.92287095715004597, -23.47593901973090169, -1.443836447538998424 ) ) ;
#52286=CARTESIAN_POINT ( 'NONE',  ( -50.02177129897295771, -25.29440776045719730, 5.833784451200525467 ) ) ;
#52287=ORIENTED_EDGE ( 'NONE', *, *, #62184, .F. ) ;
#52288=EDGE_CURVE ( 'NONE', #73698, #83369, #85640, .T. ) ;
#52289=CARTESIAN_POINT ( 'NONE',  ( -7.038884989605349141, -19.10714869031923513, -1.500000000000002220 ) ) ;
#52290=ORIENTED_EDGE ( 'NONE', *, *, #17013, .F. ) ;
#52292=CARTESIAN_POINT ( 'NONE',  ( 8.986065527603487979, -21.13286776747340667, 11.49999999999998934 ) ) ;
#52293=CARTESIAN_POINT ( 'NONE',  ( -123.6228709571500559, -29.50250786944525672, 11.44777988621622811 ) ) ;
#52295=ORIENTED_EDGE ( 'NONE', *, *, #73946, .T. ) ;
#52297=EDGE_CURVE ( 'NONE', #11909, #32345, #77781, .T. ) ;
#52298=CARTESIAN_POINT ( 'NONE',  ( -77.54282457048891786, -24.51419770103158768, 9.386484678747166299 ) ) ;
#52300=CARTESIAN_POINT ( 'NONE',  ( -87.62287095715004170, -23.47596703998600631, 11.44779298504227860 ) ) ;
#52301=CARTESIAN_POINT ( 'NONE',  ( -19.37389216307569129, 8.798533688548827669, 11.49999999999999645 ) ) ;
#52302=ORIENTED_EDGE ( 'NONE', *, *, #32289, .T. ) ;
#52304=ORIENTED_EDGE ( 'NONE', *, *, #51860, .F. ) ;
#52305=CARTESIAN_POINT ( 'NONE',  ( -0.8124730928778809425, -22.15030348749839817, 11.49999999999998934 ) ) ;
#52306=CARTESIAN_POINT ( 'NONE',  ( -15.36756058500021282, 13.76162614515376426, -1.500000000000002220 ) ) ;
#52307=VERTEX_POINT ( 'NONE', #16125 ) ;
#52308=AXIS2_PLACEMENT_3D ( 'NONE', #45529, #36905, #97801 ) ;
#52310=FACE_OUTER_BOUND ( 'NONE', #41859, .T. ) ;
#52311=EDGE_CURVE ( 'NONE', #84261, #51872, #31804, .T. ) ;
#52312=CARTESIAN_POINT ( 'NONE',  ( -121.6228709571500701, -23.96127896941633750, -0.6493128931037788210 ) ) ;
#52313=ORIENTED_EDGE ( 'NONE', *, *, #16502, .F. ) ;
#52316=CARTESIAN_POINT ( 'NONE',  ( -124.5120815788254305, -25.30053193007085355, 4.607778174927528170 ) ) ;
#52317=CARTESIAN_POINT ( 'NONE',  ( -41.48140342314091100, -24.66019654487199375, 8.947790411086124607 ) ) ;
#52319=CARTESIAN_POINT ( 'NONE',  ( 0.4431998670617953717, 20.78131286043265646, -1.500000000000002220 ) ) ;
#52320=CARTESIAN_POINT ( 'NONE',  ( 1.937016913031804455, -21.67664703184077268, 11.49999999999999645 ) ) ;
#52321=CARTESIAN_POINT ( 'NONE',  ( -50.40895856474225667, -25.03284467579915784, 7.563174216508125269 ) ) ;
#52322=CARTESIAN_POINT ( 'NONE',  ( -113.6228709571500417, -24.66019654487199730, 8.947790411086121054 ) ) ;
#52323=CARTESIAN_POINT ( 'NONE',  ( -115.6244853095894030, -24.83618233451451118, 1.606449574219534826 ) ) ;
#52324=CARTESIAN_POINT ( 'NONE',  ( 1.585521478320181865, 22.38520322874704149, -1.500000000000002220 ) ) ;
#52325=CARTESIAN_POINT ( 'NONE',  ( -51.14398700470657388, -25.26334676438652238, 4.389973610351469269 ) ) ;
#52326=VERTEX_POINT ( 'NONE', #10019 ) ;
#52327=CARTESIAN_POINT ( 'NONE',  ( -59.52287095715006160, -23.47596703998600631, 11.44779298504228926 ) ) ;
#52328=CARTESIAN_POINT ( 'NONE',  ( -51.01487234523126091, -25.13344938650803329, 2.963234457400254040 ) ) ;
#52329=B_SPLINE_SURFACE_WITH_KNOTS ( 'NONE', 3, 3, ( 
 ( #44621, #12660, #99392, #28383 ),
 ( #51737, #98892, #14151, #59855 ),
 ( #45129, #74564, #90793, #21261 ),
 ( #60855, #5053, #66975, #52236 ),
 ( #83165, #13649, #75546, #6554 ),
 ( #15157, #86672, #9548, #7551 ),
 ( #78545, #61356, #93782, #47627 ),
 ( #434, #17160, #24276, #32389 ),
 ( #31389, #8552, #46124, #92776 ),
 ( #38503, #69452, #92280, #54741 ) ),
 .UNSPECIFIED., .F., .F., .F.,
 ( 4, 3, 3, 4 ),
 ( 4, 4 ),
 ( 0.0004766839783820097840, 0.1491231665100171411, 0.2234464077758346878, 0.2977696490416522623 ),
 ( 0.2995301736809518056, 0.3007213872290413481 ),
 .UNSPECIFIED. ) ;
#52330=ORIENTED_EDGE ( 'NONE', *, *, #41424, .T. ) ;
#52331=ORIENTED_EDGE ( 'NONE', *, *, #69713, .F. ) ;
#52332=CARTESIAN_POINT ( 'NONE',  ( -99.30055519532314179, -25.26880003473793934, 6.071376037430450623 ) ) ;
#52335=CARTESIAN_POINT ( 'NONE',  ( -9.505907188867841029, -19.02311915605711690, -1.500000000000002220 ) ) ;
#52338=CARTESIAN_POINT ( 'NONE',  ( 7.388015978253313243, 19.69965359013245632, 11.49999999999998934 ) ) ;
#52340=CARTESIAN_POINT ( 'NONE',  ( -2.919094682108430483, 22.50186656173435296, 11.49999999999998934 ) ) ;
#52341=CARTESIAN_POINT ( 'NONE',  ( -113.5228709571500616, -23.47596703998600631, 11.44779298504228038 ) ) ;
#52343=CARTESIAN_POINT ( 'NONE',  ( -12.46176837856299002, 18.05058065364367792, -1.500000000000002220 ) ) ;
#52344=DIRECTION ( 'NONE',  ( 0.000000000000000000, 0.9999999999976377785, 2.173523156925979975E-06 ) ) ;
#52345=EDGE_LOOP ( 'NONE', ( #38680, #12719, #25989, #55094 ) ) ;
#52346=CARTESIAN_POINT ( 'NONE',  ( -122.5894804180817914, -24.35071581493544102, 9.817618358456019934 ) ) ;
#52348=EDGE_CURVE ( 'NONE', #55090, #62812, #33065, .T. ) ;
#52349=CARTESIAN_POINT ( 'NONE',  ( -120.5228709571500900, -24.51163499207180507, 0.6490370598555513793 ) ) ;
#52351=CARTESIAN_POINT ( 'NONE',  ( -126.9228709571500815, -23.47596703998600631, 11.44779298504227860 ) ) ;
#52353=CARTESIAN_POINT ( 'NONE',  ( 13.65650298889772962, 16.33668418983593185, 11.49999999999998934 ) ) ;
#52354=CARTESIAN_POINT ( 'NONE',  ( -112.5188950414697615, -23.96119346886881729, -0.6495511937831841554 ) ) ;
#52355=FACE_OUTER_BOUND ( 'NONE', #36700, .T. ) ;
#52357=DIRECTION ( 'NONE',  ( -0.6177208787939548751, -1.709253021876320418E-06, 0.7863974287210651060 ) ) ;
#52358=CARTESIAN_POINT ( 'NONE',  ( -33.59407879448789203, -24.15543982623906771, -0.2315651400026580431 ) ) ;
#52359=CARTESIAN_POINT ( 'NONE',  ( -117.6270234476128991, -23.96169478059714564, 10.65365249895717170 ) ) ;
#52361=CARTESIAN_POINT ( 'NONE',  ( -98.97790923573467126, -25.21099978369031902, 6.596929975353639009 ) ) ;
#52362=CARTESIAN_POINT ( 'NONE',  ( 15.22544387773384500, -12.34335808662847178, 11.49999999999999645 ) ) ;
#52363=CARTESIAN_POINT ( 'NONE',  ( -75.52287095715006160, -24.99156044556120548, 7.747789690856173195 ) ) ;
#52364=CARTESIAN_POINT ( 'NONE',  ( -129.6228709571500701, -23.48786465467241769, 11.44779295918253581 ) ) ;
#52366=CARTESIAN_POINT ( 'NONE',  ( -68.94158865110078693, -25.25654263764466023, 6.096958949246902293 ) ) ;
#52368=CARTESIAN_POINT ( 'NONE',  ( -31.62287095715004526, -24.33832256526967797, 0.1851278514119824858 ) ) ;
#52370=CARTESIAN_POINT ( 'NONE',  ( -106.5228709571500900, -23.96127896941632329, -0.6493128931037995821 ) ) ;
#52371=CARTESIAN_POINT ( 'NONE',  ( -16.05533900033903549, 11.45903963230415101, -1.500000000000002220 ) ) ;
#52374=DIRECTION ( 'NONE',  ( 0.000000000000000000, -0.9999999999976377785, -2.173523156925979975E-06 ) ) ;
#52376=B_SPLINE_CURVE_WITH_KNOTS ( 'NONE', 3,
 ( #67085, #92386, #97995, #28496, #60470, #90402 ),
 .UNSPECIFIED., .F., .F.,
 ( 4, 2, 4 ),
 ( 6.384118678602582405E-06, 0.001386860460828368046, 0.002767336802978133219 ),
 .UNSPECIFIED. ) ;
#52377=AXIS2_PLACEMENT_3D ( 'NONE', #93680, #93179, #39900 ) ;
#52379=ORIENTED_EDGE ( 'NONE', *, *, #71943, .T. ) ;
#52382=CARTESIAN_POINT ( 'NONE',  ( -55.57509554726114231, -25.00158670708910336, 2.256160236439221034 ) ) ;
#52383=CARTESIAN_POINT ( 'NONE',  ( -118.6249414734990637, -24.34968618360934300, 0.1864209137778906622 ) ) ;
#52384=CARTESIAN_POINT ( 'NONE',  ( -31.62287095715005236, -24.64965695001467694, 8.947790433994189385 ) ) ;
#52388=CARTESIAN_POINT ( 'NONE',  ( 15.90762396150235958, 12.10710967819287198, -1.500000000000002220 ) ) ;
#52389=LINE ( 'NONE', #14306, #59725 ) ;
#52390=CARTESIAN_POINT ( 'NONE',  ( -45.62923257921450215, -24.83644354573578283, 8.397322867130103674 ) ) ;
#52392=FACE_OUTER_BOUND ( 'NONE', #64446, .T. ) ;
#52395=CARTESIAN_POINT ( 'NONE',  ( -80.49780302488923667, -24.73531770709095312, 8.716586749053508498 ) ) ;
#52396=CARTESIAN_POINT ( 'NONE',  ( -125.7763423481509903, -25.21288808264143455, 6.500921239251876926 ) ) ;
#52397=CARTESIAN_POINT ( 'NONE',  ( -39.53919957490392534, -24.34968618360933235, 0.1864209137778788106 ) ) ;
#52398=DIRECTION ( 'NONE',  ( -3.773278334453079030E-23, 0.9999999999976377785, 2.173523156925979128E-06 ) ) ;
#52402=CARTESIAN_POINT ( 'NONE',  ( -127.5210452836834349, -24.51314013834318217, 0.6176544820404269442 ) ) ;
#52403=VERTEX_POINT ( 'NONE', #86143 ) ;
#52404=ADVANCED_FACE ( 'NONE', ( #71938 ), #78514, .T. ) ;
#52405=CARTESIAN_POINT ( 'NONE',  ( -3.766600276044322904, -19.90762401167813067, -1.500000000000002220 ) ) ;
#52406=CARTESIAN_POINT ( 'NONE',  ( -122.5557273655149118, -23.96119346886880663, -0.6495511937832028071 ) ) ;
#52411=EDGE_CURVE ( 'NONE', #884, #11305, #35410, .T. ) ;
#52414=CARTESIAN_POINT ( 'NONE',  ( -46.52287095715006160, -23.47596703998600631, 11.44779298504229104 ) ) ;
#52415=CARTESIAN_POINT ( 'NONE',  ( -0.3114230556345199963, -20.10660241673355486, -1.500000000000002220 ) ) ;
#52418=CARTESIAN_POINT ( 'NONE',  ( -17.44821286160079410, -11.81026508430653088, 11.49999999999999645 ) ) ;
#52419=CARTESIAN_POINT ( 'NONE',  ( -79.52287095715006160, -29.50250786944525672, 11.44777988621623521 ) ) ;
#52420=CARTESIAN_POINT ( 'NONE',  ( -70.51358061702791247, -23.85049219812685806, 10.88485053497527311 ) ) ;
#52421=CARTESIAN_POINT ( 'NONE',  ( 17.94654606563480215, 12.89224558282342947, -1.500000000000002220 ) ) ;
#52422=EDGE_CURVE ( 'NONE', #42104, #90352, #41517, .T. ) ;
#52423=CARTESIAN_POINT ( 'NONE',  ( -14.38416181709762043, 14.64695106392160895, 11.49999999999998934 ) ) ;
#52425=CARTESIAN_POINT ( 'NONE',  ( -55.58953762381671737, -24.99132157543083821, 2.256160258750496084 ) ) ;
#52426=CARTESIAN_POINT ( 'NONE',  ( -125.6228709571500559, -23.47596703998600631, 11.44779298504227860 ) ) ;
#52428=CARTESIAN_POINT ( 'NONE',  ( -27.70544111104076990, -24.64017222881049207, 8.251826729410561612 ) ) ;
#52431=ORIENTED_EDGE ( 'NONE', *, *, #37536, .F. ) ;
#52433=CARTESIAN_POINT ( 'NONE',  ( -71.62287095715004170, -24.50321055353806443, 9.387540953477532923 ) ) ;
#52435=EDGE_CURVE ( 'NONE', #923, #86931, #54812, .T. ) ;
#52436=CARTESIAN_POINT ( 'NONE',  ( -18.11865614447288664, 9.752654332028551920, -1.500000000000002220 ) ) ;
#52437=CARTESIAN_POINT ( 'NONE',  ( 20.98369277809155165, -4.918611649023987731, 11.49999999999999645 ) ) ;
#52439=DIRECTION ( 'NONE',  ( 3.773278334444167608E-23, -1.000000000000000000, 0.000000000000000000 ) ) ;
#52441=CARTESIAN_POINT ( 'NONE',  ( 21.86734719908870872, 4.625976558377421277, -1.500000000000002220 ) ) ;
#52442=VECTOR ( 'NONE', #62089, 1000.000000000000114 ) ;
#52443=DIRECTION ( 'NONE',  ( 0.000000000000000000, -0.9999999999976377785, -2.173523156925979128E-06 ) ) ;
#52444=CARTESIAN_POINT ( 'NONE',  ( -84.64006920983196380, -23.73766607897669445, -1.055555164236457566 ) ) ;
#52445=ORIENTED_EDGE ( 'NONE', *, *, #63095, .F. ) ;
#52447=CARTESIAN_POINT ( 'NONE',  ( -35.46876340121657023, -24.92592662359560407, 8.075495903017991139 ) ) ;
#52448=CARTESIAN_POINT ( 'NONE',  ( -10.06633388967972209, 18.29571535785830960, 11.49999999999998934 ) ) ;
#52450=FACE_OUTER_BOUND ( 'NONE', #90588, .T. ) ;
#52452=ORIENTED_EDGE ( 'NONE', *, *, #30758, .F. ) ;
#52454=CARTESIAN_POINT ( 'NONE',  ( -100.6255024803089384, -24.83644354573579349, 8.397322867130096569 ) ) ;
#52455=CARTESIAN_POINT ( 'NONE',  ( 6.686094007546604878, -20.02240253118446844, -1.500000000000002220 ) ) ;
#52456=ORIENTED_EDGE ( 'NONE', *, *, #6982, .F. ) ;
#52457=CARTESIAN_POINT ( 'NONE',  ( -117.5535922921180543, -24.34968618360934656, 0.1864209137778901071 ) ) ;
#52458=CARTESIAN_POINT ( 'NONE',  ( -35.58953762381671737, -25.00182538069144655, 7.747789668545102870 ) ) ;
#52459=CARTESIAN_POINT ( 'NONE',  ( -19.23829340896090656, 10.21096329589227025, 11.49999999999998934 ) ) ;
#52460=CARTESIAN_POINT ( 'NONE',  ( -110.2414738297690775, -25.25449932609592096, 6.186391010255299250 ) ) ;
#52463=CARTESIAN_POINT ( 'NONE',  ( -80.11765714520616655, -25.14277807208376458, 7.046040345931035453 ) ) ;
#52464=CARTESIAN_POINT ( 'NONE',  ( 20.57166443188586769, -7.073620337204646447, -1.500000000000002220 ) ) ;
#52465=CARTESIAN_POINT ( 'NONE',  ( -106.5228709571500758, -23.48786465467242479, 11.44779295918253936 ) ) ;
#52466=CARTESIAN_POINT ( 'NONE',  ( -10.28394192611005842, 19.82837715243953625, 11.49999999999999645 ) ) ;
#52467=ORIENTED_EDGE ( 'NONE', *, *, #65844, .T. ) ;
#52468=CARTESIAN_POINT ( 'NONE',  ( -45.62287095715007723, -24.83602698348160231, 1.605859176311266623 ) ) ;
#52470=ADVANCED_FACE ( 'NONE', ( #3926 ), #12016, .F. ) ;
#52471=CARTESIAN_POINT ( 'NONE',  ( -77.62287095715007013, -23.48783264082478794, -1.443836473390065933 ) ) ;
#52473=ORIENTED_EDGE ( 'NONE', *, *, #24455, .F. ) ;
#52474=EDGE_CURVE ( 'NONE', #91631, #49598, #72973, .T. ) ;
#52479=CARTESIAN_POINT ( 'NONE',  ( -43.62287095715003460, -23.47596703998600276, 11.44779298504227505 ) ) ;
#52480=LINE ( 'NONE', #46356, #31381 ) ;
#52481=CARTESIAN_POINT ( 'NONE',  ( -4.359330469889163950, 18.88329184224734192, -1.500000000000002220 ) ) ;
#52482=EDGE_CURVE ( 'NONE', #62581, #24865, #2695, .T. ) ;
#52483=CARTESIAN_POINT ( 'NONE',  ( -103.6228709571500559, -24.64898659630368627, 1.056161002820829697 ) ) ;
#52485=CARTESIAN_POINT ( 'NONE',  ( 19.04819733361787470, -3.913502273677552878, 11.49999999999999645 ) ) ;
#52486=CARTESIAN_POINT ( 'NONE',  ( -88.22287095715006444, -23.47596703998600631, 11.44779298504227860 ) ) ;
#52488=VERTEX_POINT ( 'NONE', #42495 ) ;
#52492=CARTESIAN_POINT ( 'NONE',  ( -116.5228709571500474, -24.33832256527048088, 0.1851278514138653408 ) ) ;
#52493=CARTESIAN_POINT ( 'NONE',  ( -63.94589268014165384, -23.78087380709146004, 10.97511746239721298 ) ) ;
#52494=CARTESIAN_POINT ( 'NONE',  ( 18.19143915067776263, 7.407926943018095400, 11.49999999999998934 ) ) ;
#52496=CARTESIAN_POINT ( 'NONE',  ( -46.54684453743023198, -24.15543982623906771, -0.2315651400026683127 ) ) ;
#52498=CARTESIAN_POINT ( 'NONE',  ( 0.7969447072908428797, -21.54811710690876225, -1.500000000000002220 ) ) ;
#52500=CARTESIAN_POINT ( 'NONE',  ( -115.9228709571500815, -23.47593901973090524, -1.443836447538996426 ) ) ;
#52502=CARTESIAN_POINT ( 'NONE',  ( -99.59031406714542811, -25.18439430774925114, 3.731155517086302886 ) ) ;
#52503=CARTESIAN_POINT ( 'NONE',  ( 8.428894486204411507, 21.44871590506140890, -1.500000000000002220 ) ) ;
#52507=CARTESIAN_POINT ( 'NONE',  ( -50.10007593363737044, -25.29249258120279009, 4.255736650380444352 ) ) ;
#52508=CARTESIAN_POINT ( 'NONE',  ( 17.11712468798820908, 10.61635618877791742, 11.49999999999999645 ) ) ;
#52512=DIRECTION ( 'NONE',  ( 0.000000000000000000, 0.9999999999976377785, 2.173523156925979975E-06 ) ) ;
#52513=CARTESIAN_POINT ( 'NONE',  ( -110.7296117302316532, -25.18425597211279410, 3.360883082042677383 ) ) ;
#52514=CARTESIAN_POINT ( 'NONE',  ( 4.721227339208565965, -19.33841413273825793, -1.500000000000002220 ) ) ;
#52515=CARTESIAN_POINT ( 'NONE',  ( -113.5205660264642802, -23.73766607897670866, -1.055555164236448240 ) ) ;
#52516=CARTESIAN_POINT ( 'NONE',  ( 18.24634267693259559, -7.554628487255452107, -1.500000000000002220 ) ) ;
#52518=LINE ( 'NONE', #5342, #67829 ) ;
#52520=CARTESIAN_POINT ( 'NONE',  ( 11.71144010791963730, -17.07555522294065753, 11.49999999999999645 ) ) ;
#52521=CARTESIAN_POINT ( 'NONE',  ( -98.62287095715005592, -24.64898659630529210, 1.056161002820829697 ) ) ;
#52523=CARTESIAN_POINT ( 'NONE',  ( -128.5228709571500758, -24.64965694238575722, 8.947790433994189385 ) ) ;
#52524=CARTESIAN_POINT ( 'NONE',  ( 12.08046422559826816, 19.21373320108137861, 11.49999999999999645 ) ) ;
#52525=ORIENTED_EDGE ( 'NONE', *, *, #66303, .F. ) ;
#52526=CARTESIAN_POINT ( 'NONE',  ( -78.55620429048339304, -24.65952944569304606, 1.056160979905699904 ) ) ;
#52528=CARTESIAN_POINT ( 'NONE',  ( 3.569899647507075890, 19.86734082857295647, 11.49999999999998934 ) ) ;
#52529=EDGE_CURVE ( 'NONE', #13388, #46438, #73922, .T. ) ;
#52530=CARTESIAN_POINT ( 'NONE',  ( -63.49958784806312906, -24.34968618360933235, 0.1864209137778804204 ) ) ;
#52531=CARTESIAN_POINT ( 'NONE',  ( -52.52287095715006870, -23.47596703998600631, 11.44779298504229104 ) ) ;
#52532=EDGE_LOOP ( 'NONE', ( #57937, #8352, #53076, #54774 ) ) ;
#52533=ORIENTED_EDGE ( 'NONE', *, *, #18024, .T. ) ;
#52535=CARTESIAN_POINT ( 'NONE',  ( 11.15996004898972771, 19.99216496293481882, 11.49999999999998934 ) ) ;
#52536=CARTESIAN_POINT ( 'NONE',  ( -29.51208538039775320, -23.65073901887618391, -1.055554856561816246 ) ) ;
#52537=CARTESIAN_POINT ( 'NONE',  ( -4.138935798035190849, -21.16376344109877294, -1.500000000000002220 ) ) ;
#52538=CARTESIAN_POINT ( 'NONE',  ( -123.5890690777296754, -24.51314013834316796, 0.6176544820404235026 ) ) ;
#52539=CARTESIAN_POINT ( 'NONE',  ( -34.57522798308936984, -24.65952944569304606, 1.056160979905694353 ) ) ;
#52540=EDGE_CURVE ( 'NONE', #72780, #83889, #13632, .T. ) ;
#52541=CARTESIAN_POINT ( 'NONE',  ( 6.973883220674568229, 19.69035807221911938, 11.49999999999999645 ) ) ;
#52543=CARTESIAN_POINT ( 'NONE',  ( -27.75896112051811926, -24.78822140492940918, 2.278705362813905122 ) ) ;
#52544=CARTESIAN_POINT ( 'NONE',  ( 13.70243205411677145, -17.22335469805116048, 11.49999999999998934 ) ) ;
#52545=EDGE_CURVE ( 'NONE', #24081, #26377, #12377, .T. ) ;
#52548=CARTESIAN_POINT ( 'NONE',  ( -41.86772617331516955, -25.10926054140117003, 4.147750411746549126 ) ) ;
#52551=CARTESIAN_POINT ( 'NONE',  ( -90.50269173505331821, -24.73531770709095312, 8.716586749053512051 ) ) ;
#52552=ORIENTED_EDGE ( 'NONE', *, *, #63488, .T. ) ;
#52553=DIRECTION ( 'NONE',  ( -3.773278334453079030E-23, 0.9999999999976377785, 2.173523156925979128E-06 ) ) ;
#52554=B_SPLINE_CURVE_WITH_KNOTS ( 'NONE', 3,
 ( #9061, #46638, #31902, #62359, #93285, #79065 ),
 .UNSPECIFIED., .F., .F.,
 ( 4, 2, 4 ),
 ( 1.570755371634190273E-05, 0.001396183895866089054, 0.002776660238015836446 ),
 .UNSPECIFIED. ) ;
#52555=EDGE_LOOP ( 'NONE', ( #67961, #10491, #26344, #11374 ) ) ;
#52557=CARTESIAN_POINT ( 'NONE',  ( -71.54508653244631944, -24.35071581493543391, 9.817618358456021710 ) ) ;
#52558=CARTESIAN_POINT ( 'NONE',  ( -42.52287095715005449, -29.50248528299804818, 1.056150453629031594 ) ) ;
#52559=CARTESIAN_POINT ( 'NONE',  ( -36.52201406890371516, -23.48783264082477018, -1.443836473390095909 ) ) ;
#52561=CARTESIAN_POINT ( 'NONE',  ( 17.64890103348723116, 10.21726211432410203, -1.500000000000002220 ) ) ;
#52562=B_SPLINE_CURVE_WITH_KNOTS ( 'NONE', 3,
 ( #11795, #37130, #51366, #67106, #28515, #66118 ),
 .UNSPECIFIED., .F., .F.,
 ( 4, 2, 4 ),
 ( 1.570887131794638196E-05, 0.001396322306279760422, 0.002776935741241574537 ),
 .UNSPECIFIED. ) ;
#52564=ORIENTED_EDGE ( 'NONE', *, *, #53233, .F. ) ;
#52568=CARTESIAN_POINT ( 'NONE',  ( -25.53602269318328055, -24.91361206832937469, 5.313022737699515829 ) ) ;
#52571=CARTESIAN_POINT ( 'NONE',  ( -29.12273499046074221, -25.26247934485601832, 7.596950907507011408 ) ) ;
#52572=CARTESIAN_POINT ( 'NONE',  ( 14.06386034339543478, -15.33156129944631729, 11.49999999999998934 ) ) ;
#52575=EDGE_LOOP ( 'NONE', ( #66449, #5146, #53719, #10365 ) ) ;
#52576=LINE ( 'NONE', #20123, #79521 ) ;
#52577=ORIENTED_EDGE ( 'NONE', *, *, #50823, .T. ) ;
#52578=EDGE_LOOP ( 'NONE', ( #56312, #50390, #50599, #77484 ) ) ;
#52580=CARTESIAN_POINT ( 'NONE',  ( -117.0508404609613251, -25.24693487555287064, 3.801655821953186631 ) ) ;
#52582=CARTESIAN_POINT ( 'NONE',  ( -99.64934318012689118, -29.50249369713380077, 4.927347193923941049 ) ) ;
#52583=CARTESIAN_POINT ( 'NONE',  ( -16.97254739485517661, -14.18817111035334655, 11.49999999999999645 ) ) ;
#52585=FACE_OUTER_BOUND ( 'NONE', #64697, .T. ) ;
#52586=CARTESIAN_POINT ( 'NONE',  ( 17.19246737676917292, 14.74310579602587090, -1.500000000000002220 ) ) ;
#52587=CARTESIAN_POINT ( 'NONE',  ( -92.52287095715006160, -24.34917612407051379, 0.1852690917482314736 ) ) ;
#52589=EDGE_CURVE ( 'NONE', #82121, #82898, #49601, .T. ) ;
#52590=ORIENTED_EDGE ( 'NONE', *, *, #58665, .F. ) ;
#52592=B_SPLINE_CURVE_WITH_KNOTS ( 'NONE', 3,
 ( #88870, #19340, #81243, #12218, #43195, #74135 ),
 .UNSPECIFIED., .F., .F.,
 ( 4, 2, 4 ),
 ( 0.000000000000000000, 0.001380764517854764532, 0.002761529035709529064 ),
 .UNSPECIFIED. ) ;
#52596=CARTESIAN_POINT ( 'NONE',  ( -4.889416449700032530, -19.50743224814450016, -1.500000000000002220 ) ) ;
#52597=B_SPLINE_SURFACE_WITH_KNOTS ( 'NONE', 3, 3, ( 
 ( #3991, #74001, #41561, #4494 ),
 ( #18211, #49183, #88231, #94831 ),
 ( #34934, #80107, #96827, #87219 ),
 ( #17713, #72509, #48683, #3002 ),
 ( #50169, #79606, #41055, #11587 ),
 ( #49677, #80604, #11096, #42564 ),
 ( #37432, #99315, #74488, #60779 ),
 ( #82107, #14076, #83085, #84094 ),
 ( #97330, #90716, #66410, #58771 ),
 ( #45550, #12588, #29808, #97821 ) ),
 .UNSPECIFIED., .F., .F., .F.,
 ( 4, 3, 3, 4 ),
 ( 4, 4 ),
 ( 0.7022005934544808259, 0.7765311282028795059, 0.8508616629512781859, 0.9995227324480754350 ),
 ( 0.1995180756172104108, 0.2006497107716917472 ),
 .UNSPECIFIED. ) ;
#52598=CARTESIAN_POINT ( 'NONE',  ( -36.62287095715004170, -23.47596703998600276, 11.44779298504227505 ) ) ;
#52599=ORIENTED_EDGE ( 'NONE', *, *, #56569, .T. ) ;
#52601=CARTESIAN_POINT ( 'NONE',  ( 5.437191932089902480, -21.69250089042843754, -1.500000000000002220 ) ) ;
#52602=ORIENTED_EDGE ( 'NONE', *, *, #1438, .F. ) ;
#52603=ORIENTED_EDGE ( 'NONE', *, *, #4292, .T. ) ;
#52605=DIRECTION ( 'NONE',  ( -3.773278334453079618E-23, 0.9999999999976377785, 2.173523156925979975E-06 ) ) ;
#52607=CARTESIAN_POINT ( 'NONE',  ( -96.62287095715005592, -23.48786465467241413, 11.44779295918254114 ) ) ;
#52609=CARTESIAN_POINT ( 'NONE',  ( 0.4223197742854877812, 19.52780805513575402, -1.500000000000002220 ) ) ;
#52610=CARTESIAN_POINT ( 'NONE',  ( -47.52287095715006160, -24.65952944569304606, 1.056160979905693686 ) ) ;
#52611=CARTESIAN_POINT ( 'NONE',  ( -16.43003769262999469, -13.82051474754189258, 11.49999999999998934 ) ) ;
#52612=CARTESIAN_POINT ( 'NONE',  ( -25.53214279450137170, -24.58000196289700057, 4.846047347457761667 ) ) ;
#52613=CARTESIAN_POINT ( 'NONE',  ( -90.52287095715006160, -29.50248789122583659, 2.256150453626215580 ) ) ;
#52614=LINE ( 'NONE', #28777, #40940 ) ;
#52615=CARTESIAN_POINT ( 'NONE',  ( 4.317061085376620255, -22.40314112565372540, -1.500000000000002220 ) ) ;
#52616=VECTOR ( 'NONE', #12203, 1000.000000000000114 ) ;
#52619=CARTESIAN_POINT ( 'NONE',  ( -96.51073854974256960, -24.35071581493543391, 9.817618358456023486 ) ) ;
#52621=CARTESIAN_POINT ( 'NONE',  ( -12.72357806474857966, 15.40231687525621318, 11.49999999999999645 ) ) ;
#52622=LINE ( 'NONE', #53637, #92167 ) ;
#52623=CARTESIAN_POINT ( 'NONE',  ( -74.58126559791662658, -24.66019654487199730, 8.947790411086108620 ) ) ;
#52625=ORIENTED_EDGE ( 'NONE', *, *, #57672, .F. ) ;
#52626=CARTESIAN_POINT ( 'NONE',  ( -56.62287095715005592, -23.47593901973091235, -1.443836447539007972 ) ) ;
#52629=CARTESIAN_POINT ( 'NONE',  ( -6.878457297428972161, 20.61903435171069532, 11.49999999999998934 ) ) ;
#52631=CARTESIAN_POINT ( 'NONE',  ( -66.22287095715006444, -23.47596703998600276, 11.44779298504227860 ) ) ;
#52632=CARTESIAN_POINT ( 'NONE',  ( -10.82925958622295859, 16.30987832687952022, -1.500000000000002220 ) ) ;
#52633=CARTESIAN_POINT ( 'NONE',  ( -100.3728165607841447, -25.13336937450139175, 7.100323077445898079 ) ) ;
#52634=B_SPLINE_CURVE_WITH_KNOTS ( 'NONE', 3,
 ( #63860, #94774, #9040, #93774, #92766, #54234 ),
 .UNSPECIFIED., .F., .F.,
 ( 4, 2, 4 ),
 ( 6.384118678617699402E-06, 0.001386860460828380189, 0.002767336802978142760 ),
 .UNSPECIFIED. ) ;
#52635=EDGE_LOOP ( 'NONE', ( #63322, #65187, #5874, #31984 ) ) ;
#52636=ADVANCED_FACE ( 'NONE', ( #60703 ), #84516, .T. ) ;
#52639=CARTESIAN_POINT ( 'NONE',  ( 18.57849760351508195, 8.651319581928444080, 11.49999999999999645 ) ) ;
#52641=CARTESIAN_POINT ( 'NONE',  ( -40.58953762381673158, -23.48783264082478084, -1.443836473390072817 ) ) ;
#52642=B_SPLINE_CURVE_WITH_KNOTS ( 'NONE', 3,
 ( #16977, #38316, #61185, #23580, #92106, #22573, #77864, #78864 ),
 .UNSPECIFIED., .F., .F.,
 ( 4, 2, 2, 4 ),
 ( -0.001240355328176663422, -0.0002398155169398021556, 0.0007607242942970591105, 0.002761803916770780992 ),
 .UNSPECIFIED. ) ;
#52643=ORIENTED_EDGE ( 'NONE', *, *, #73738, .F. ) ;
#52646=FACE_OUTER_BOUND ( 'NONE', #65061, .T. ) ;
#52648=CARTESIAN_POINT ( 'NONE',  ( -85.62287095715005592, -29.50247984919015209, -1.443849546365051806 ) ) ;
#52649=ORIENTED_EDGE ( 'NONE', *, *, #77818, .F. ) ;
#52651=CARTESIAN_POINT ( 'NONE',  ( -10.12245940999746985, -20.73198382670940987, 11.49999999999999645 ) ) ;
#52652=CARTESIAN_POINT ( 'NONE',  ( -7.601706241105644857, -21.46296766604531570, -1.500000000000002220 ) ) ;
#52653=CARTESIAN_POINT ( 'NONE',  ( -70.50669286463424612, -25.31517374732275982, 4.857674065044717437 ) ) ;
#52654=CARTESIAN_POINT ( 'NONE',  ( -105.6228709571500559, -24.91544648472627088, 1.928969306349436197 ) ) ;
#52655=CARTESIAN_POINT ( 'NONE',  ( -98.52287095715007581, -23.47593901973090524, -1.443836447538996648 ) ) ;
#52658=CARTESIAN_POINT ( 'NONE',  ( -110.6301004589282115, -24.15503026093913519, -0.2815557561904549755 ) ) ;
#52659=CARTESIAN_POINT ( 'NONE',  ( 11.09338859787202480, -18.89396691112096605, 11.49999999999998934 ) ) ;
#52660=ADVANCED_FACE ( 'NONE', ( #83012 ), #23100, .T. ) ;
#52663=CARTESIAN_POINT ( 'NONE',  ( -50.62287095715007723, -24.83602698348159876, 1.605859176311268177 ) ) ;
#52664=CARTESIAN_POINT ( 'NONE',  ( -41.42859576553861700, -25.30281640502126095, 4.441720959794929868 ) ) ;
#52666=CARTESIAN_POINT ( 'NONE',  ( -78.55032942013556863, -24.15543982623907127, -0.2315651400026641771 ) ) ;
#52667=CARTESIAN_POINT ( 'NONE',  ( -112.6228709571500559, -24.64898659630368272, 1.056161002820831474 ) ) ;
#52668=CARTESIAN_POINT ( 'NONE',  ( -107.6228709571500701, -24.64965695001469115, 8.947790433994176951 ) ) ;
#52670=CARTESIAN_POINT ( 'NONE',  ( -4.302178748239556150, -20.00421716419250373, -1.500000000000002220 ) ) ;
#52671=VERTEX_POINT ( 'NONE', #6403 ) ;
#52673=ORIENTED_EDGE ( 'NONE', *, *, #69956, .T. ) ;
#52675=CARTESIAN_POINT ( 'NONE',  ( 21.63105218614105851, 7.968772182826888262, 11.49999999999998934 ) ) ;
#52676=CARTESIAN_POINT ( 'NONE',  ( -35.52287095715006160, -24.83602698348240878, 1.605859176314146763 ) ) ;
#52677=EDGE_CURVE ( 'NONE', #41225, #24356, #75399, .T. ) ;
#52678=CARTESIAN_POINT ( 'NONE',  ( 6.697674113365701842, 19.09646837838083400, -1.500000000000002220 ) ) ;
#52679=EDGE_LOOP ( 'NONE', ( #42161, #43719, #72400, #45699 ) ) ;
#52680=CARTESIAN_POINT ( 'NONE',  ( -90.52287095715003318, -25.00182538069145366, 7.747789668545104647 ) ) ;
#52681=PLANE ( 'NONE',  #22236 ) ;
#52683=CARTESIAN_POINT ( 'NONE',  ( -127.6228709571500559, -23.47596703998600631, 11.44779298504227860 ) ) ;
#52684=CARTESIAN_POINT ( 'NONE',  ( -99.63465650044997801, -23.73791477778911840, 11.05961554403170410 ) ) ;
#52685=CARTESIAN_POINT ( 'NONE',  ( -2.231587876719630437, -21.34735720706076378, 11.49999999999999645 ) ) ;
#52687=CARTESIAN_POINT ( 'NONE',  ( -128.6228709571500417, -23.47593901973091235, -1.443836447538995760 ) ) ;
#52690=CARTESIAN_POINT ( 'NONE',  ( -1.843323519027639357, -20.62917239659568835, -1.500000000000002220 ) ) ;
#52691=AXIS2_PLACEMENT_3D ( 'NONE', #11595, #33438, #3999 ) ;
#52692=B_SPLINE_CURVE_WITH_KNOTS ( 'NONE', 3,
 ( #9466, #43298, #2366, #56661 ),
 .UNSPECIFIED., .F., .F.,
 ( 4, 4 ),
 ( 2.778582473997085907E-06, 0.0004643190030723578360 ),
 .UNSPECIFIED. ) ;
#52693=CARTESIAN_POINT ( 'NONE',  ( -80.62287095715004170, -23.48783264082478439, -1.443836473390065489 ) ) ;
#52694=VERTEX_POINT ( 'NONE', #5897 ) ;
#52695=CARTESIAN_POINT ( 'NONE',  ( -28.64432147930652661, -24.00272683650521088, -0.2315644524145782090 ) ) ;
#52698=ORIENTED_EDGE ( 'NONE', *, *, #20476, .T. ) ;
#52699=CARTESIAN_POINT ( 'NONE',  ( -20.97355972163249049, 0.1317905507124840780, -1.500000000000002220 ) ) ;
#52700=CARTESIAN_POINT ( 'NONE',  ( 12.93620265873104991, 17.78788284566447331, 11.49999999999999645 ) ) ;
#52701=VECTOR ( 'NONE', #71180, 1000.000000000000114 ) ;
#52702=CARTESIAN_POINT ( 'NONE',  ( -37.58684943389518196, -24.35071581493542325, 9.817618358456030592 ) ) ;
#52703=CARTESIAN_POINT ( 'NONE',  ( 22.38532167473930556, -2.757513164441831144, 11.49999999999998934 ) ) ;
#52705=CARTESIAN_POINT ( 'NONE',  ( -9.893913718187896222, 18.50344063021147889, 11.49999999999998934 ) ) ;
#52706=CARTESIAN_POINT ( 'NONE',  ( -48.58953762381671737, -23.48783264082478439, -1.443836473390070596 ) ) ;
#52707=B_SPLINE_CURVE_WITH_KNOTS ( 'NONE', 3,
 ( #17171, #41521, #93795, #9559, #87187, #79573 ),
 .UNSPECIFIED., .F., .F.,
 ( 4, 2, 4 ),
 ( 1.570755371634170283E-05, 0.001396183895866089488, 0.002776660238015837313 ),
 .UNSPECIFIED. ) ;
#52708=CARTESIAN_POINT ( 'NONE',  ( -45.62287095715004881, -29.50250786944525672, 11.44777988621624054 ) ) ;
#52711=ORIENTED_EDGE ( 'NONE', *, *, #67383, .F. ) ;
#52715=CARTESIAN_POINT ( 'NONE',  ( -0.8555947871142663974, 21.52075748220454798, -1.500000000000002220 ) ) ;
#52716=ADVANCED_FACE ( 'NONE', ( #29235 ), #76882, .F. ) ;
#52719=CARTESIAN_POINT ( 'NONE',  ( 13.68530018921192060, -16.06810839794082924, 11.49999999999998934 ) ) ;
#52720=DIRECTION ( 'NONE',  ( 3.773278334444167608E-23, -1.000000000000000000, 0.000000000000000000 ) ) ;
#52722=CARTESIAN_POINT ( 'NONE',  ( -83.50067839706997574, -24.66019654487199375, 8.947790411086122830 ) ) ;
#52724=CARTESIAN_POINT ( 'NONE',  ( -41.62287095715006302, -23.47593901973091235, -1.443836447539011525 ) ) ;
#52725=CARTESIAN_POINT ( 'NONE',  ( -16.08457400211760913, 15.13120210334024662, -1.500000000000002220 ) ) ;
#52727=VERTEX_POINT ( 'NONE', #91132 ) ;
#52728=FACE_OUTER_BOUND ( 'NONE', #97867, .T. ) ;
#52732=CARTESIAN_POINT ( 'NONE',  ( 16.42231304340664266, 10.40281881132301045, -1.500000000000002220 ) ) ;
#52734=CARTESIAN_POINT ( 'NONE',  ( -20.23222619987061677, -6.887663580918623296, -1.500000000000002220 ) ) ;
#52735=CARTESIAN_POINT ( 'NONE',  ( -69.47951456376665647, -25.09778000710391765, 7.297977585176790072 ) ) ;
#52737=CARTESIAN_POINT ( 'NONE',  ( -73.62287095715005592, -24.64898659630367916, 1.056161002820824368 ) ) ;
#52738=CARTESIAN_POINT ( 'NONE',  ( -36.62287095715007013, -24.35013146730203459, 9.818937971375119034 ) ) ;
#52739=CARTESIAN_POINT ( 'NONE',  ( -1.322449806865925614, 22.60218017400935864, -1.500000000000002220 ) ) ;
#52741=ORIENTED_EDGE ( 'NONE', *, *, #33526, .F. ) ;
#52742=CARTESIAN_POINT ( 'NONE',  ( -128.5895376238167103, -24.65952944569305316, 1.056160979905707897 ) ) ;
#52743=DIRECTION ( 'NONE',  ( 0.4561809899890718056, 0.000000000000000000, -0.8898870177570803452 ) ) ;
#52744=CARTESIAN_POINT ( 'NONE',  ( -2.602694502683683631, -19.63732897141692391, 11.49999999999999645 ) ) ;
#52745=B_SPLINE_CURVE_WITH_KNOTS ( 'NONE', 3,
 ( #10046, #73453, #96287, #56246, #18159, #17659 ),
 .UNSPECIFIED., .F., .F.,
 ( 4, 2, 4 ),
 ( 6.384118696097665072E-06, 0.001386860460837120376, 0.002767336802978143193 ),
 .UNSPECIFIED. ) ;
#52746=CARTESIAN_POINT ( 'NONE',  ( -94.52287095715006160, -29.50250786944525672, 11.44777988621623344 ) ) ;
#52748=CARTESIAN_POINT ( 'NONE',  ( -99.62287095715005592, -29.50250243563736774, 8.947779886222138046 ) ) ;
#52749=CARTESIAN_POINT ( 'NONE',  ( -115.6228709571500701, -25.00158670708909625, 2.256160236439165967 ) ) ;
#52751=CARTESIAN_POINT ( 'NONE',  ( -8.642975711230413083, 19.83371042614930957, -1.500000000000002220 ) ) ;
#52752=EDGE_CURVE ( 'NONE', #23327, #82927, #84015, .T. ) ;
#52753=CARTESIAN_POINT ( 'NONE',  ( -41.52287095715006870, -29.50250243563736774, 8.947779886222148704 ) ) ;
#52754=CARTESIAN_POINT ( 'NONE',  ( -11.04204518803028456, 15.98388583709530941, -1.500000000000002220 ) ) ;
#52756=CARTESIAN_POINT ( 'NONE',  ( -61.62287095715004170, -23.73907113216991505, -1.053371485793230589 ) ) ;
#52758=CARTESIAN_POINT ( 'NONE',  ( 10.49454761162020588, -16.79419365751139637, 11.49999999999998934 ) ) ;
#52759=ORIENTED_EDGE ( 'NONE', *, *, #40430, .F. ) ;
#52761=CARTESIAN_POINT ( 'NONE',  ( -8.348131891436525009, -18.51812344263101906, 11.49999999999999645 ) ) ;
#52762=CARTESIAN_POINT ( 'NONE',  ( -80.62685931099697711, -24.83618233451450408, 1.606449574219532384 ) ) ;
#52766=ORIENTED_EDGE ( 'NONE', *, *, #5101, .T. ) ;
#52767=CARTESIAN_POINT ( 'NONE',  ( -102.6335722854369266, -23.73791477778911840, 11.05961554403170410 ) ) ;
#52768=CARTESIAN_POINT ( 'NONE',  ( -116.4728709571500502, -25.21147115889351298, 5.000950864497187176 ) ) ;
#52773=CARTESIAN_POINT ( 'NONE',  ( -14.83682921977595548, 13.52632505182701017, 11.49999999999998934 ) ) ;
#52775=ADVANCED_FACE ( 'NONE', ( #32223 ), #8392, .F. ) ;
#52778=VERTEX_POINT ( 'NONE', #77887 ) ;
#52780=VECTOR ( 'NONE', #79836, 1000.000000000000114 ) ;
#52781=CARTESIAN_POINT ( 'NONE',  ( 17.58993269669914383, -14.52173041563253975, 11.49999999999999645 ) ) ;
#52782=CARTESIAN_POINT ( 'NONE',  ( -49.57368764975930731, -25.31297113922084208, 4.259411968733069820 ) ) ;
#52783=DIRECTION ( 'NONE',  ( -3.773278334453079618E-23, 0.9999999999976377785, 2.173523156925978705E-06 ) ) ;
#52784=CARTESIAN_POINT ( 'NONE',  ( -114.5895376238166961, -24.65952944569305316, 1.056160979905700570 ) ) ;
#52790=CARTESIAN_POINT ( 'NONE',  ( -20.29798418530817017, 1.744846428065259136, -1.500000000000002220 ) ) ;
#52792=CARTESIAN_POINT ( 'NONE',  ( 3.929728083993185184, -22.62717521373229701, -1.500000000000002220 ) ) ;
#52793=EDGE_CURVE ( 'NONE', #30324, #18231, #7532, .T. ) ;
#52794=FACE_OUTER_BOUND ( 'NONE', #79618, .T. ) ;
#52795=EDGE_LOOP ( 'NONE', ( #84807, #695, #61398, #85457, #38447, #71778, #77791, #92686, #27854, #64626, #63133, #68776, #14482, #33427, #61612, #38926, #48357 ) ) ;
#52796=CARTESIAN_POINT ( 'NONE',  ( -101.3869470976398333, -25.19665614377478136, 6.627173498926840267 ) ) ;
#52797=EDGE_CURVE ( 'NONE', #82714, #21186, #81406, .T. ) ;
#52798=CARTESIAN_POINT ( 'NONE',  ( -77.54619546820211440, -24.35071581493544102, 9.817618358456021710 ) ) ;
#52800=CARTESIAN_POINT ( 'NONE',  ( -51.64512824026234483, -23.96169478059713143, 10.65365249895718236 ) ) ;
#52801=CARTESIAN_POINT ( 'NONE',  ( 15.87343765641381665, 14.11872912734625274, 11.49999999999999645 ) ) ;
#52802=ORIENTED_EDGE ( 'NONE', *, *, #67835, .T. ) ;
#52804=ORIENTED_EDGE ( 'NONE', *, *, #80816, .F. ) ;
#52805=CARTESIAN_POINT ( 'NONE',  ( 10.53326394202159300, -19.55463526559320542, -1.500000000000002220 ) ) ;
#52806=CARTESIAN_POINT ( 'NONE',  ( -11.82494684808912844, 16.90534455221803967, 11.49999999999998934 ) ) ;
#52807=VERTEX_POINT ( 'NONE', #9389 ) ;
#52808=ORIENTED_EDGE ( 'NONE', *, *, #74911, .F. ) ;
#52810=EDGE_CURVE ( 'NONE', #85607, #14971, #40248, .T. ) ;
#52811=CARTESIAN_POINT ( 'NONE',  ( -40.07214526342530547, -25.12798243322264469, 2.874043696753044053 ) ) ;
#52812=VERTEX_POINT ( 'NONE', #33229 ) ;
#52813=VERTEX_POINT ( 'NONE', #15994 ) ;
#52815=FACE_OUTER_BOUND ( 'NONE', #26073, .T. ) ;
#52816=CARTESIAN_POINT ( 'NONE',  ( -18.54028579900546703, -9.471972883075929772, -1.500000000000002220 ) ) ;
#52817=CARTESIAN_POINT ( 'NONE',  ( 6.711561834375728175, -20.75310922853297058, 11.49999999999999645 ) ) ;
#52818=CARTESIAN_POINT ( 'NONE',  ( -39.58615480296015221, -25.23770002871814455, 3.714675945737659912 ) ) ;
#52819=CARTESIAN_POINT ( 'NONE',  ( -89.81226385320383088, -29.50249166729307149, 3.993452963156916002 ) ) ;
#52820=CARTESIAN_POINT ( 'NONE',  ( -3.368041826647835357, -22.21310627845187824, -1.500000000000002220 ) ) ;
#52821=CARTESIAN_POINT ( 'NONE',  ( -50.72939492065860634, -25.31296752812565387, 4.679804727249790908 ) ) ;
#52822=ORIENTED_EDGE ( 'NONE', *, *, #603, .F. ) ;
#52827=CARTESIAN_POINT ( 'NONE',  ( -46.56868764939927985, -23.48786465467240703, 11.44779295918255180 ) ) ;
#52828=EDGE_LOOP ( 'NONE', ( #24979, #53495, #86203, #55082 ) ) ;
#52830=CARTESIAN_POINT ( 'NONE',  ( 20.90283063341239966, -4.354886778353011856, -1.500000000000002220 ) ) ;
#52831=ORIENTED_EDGE ( 'NONE', *, *, #68687, .F. ) ;
#52834=CARTESIAN_POINT ( 'NONE',  ( 4.297136154115697160, 20.59472113332480703, 11.49999999999998934 ) ) ;
#52835=CARTESIAN_POINT ( 'NONE',  ( -30.54993633120672314, -24.48461703701380543, 0.5642940035406466270 ) ) ;
#52836=CARTESIAN_POINT ( 'NONE',  ( -41.46524908126663433, -25.18431059086284307, 4.157779966712787711 ) ) ;
#52837=CARTESIAN_POINT ( 'NONE',  ( -79.11611000704996854, -25.15699314367416051, 3.101158825156976828 ) ) ;
#52838=CARTESIAN_POINT ( 'NONE',  ( -17.52905966558703454, -13.16386835867055716, -1.500000000000002220 ) ) ;
#52840=ORIENTED_EDGE ( 'NONE', *, *, #40173, .T. ) ;
#52841=B_SPLINE_CURVE_WITH_KNOTS ( 'NONE', 3,
 ( #62139, #31672, #16440, #40294, #47911, #25056 ),
 .UNSPECIFIED., .F., .F.,
 ( 4, 2, 4 ),
 ( 1.570755371633777598E-05, 0.001396183895866085151, 0.002776660238015832543 ),
 .UNSPECIFIED. ) ;
#52842=CARTESIAN_POINT ( 'NONE',  ( -122.5214654115758037, -23.73791477778912551, 11.05961554403169878 ) ) ;
#52844=VECTOR ( 'NONE', #79851, 1000.000000000000114 ) ;
#52845=CARTESIAN_POINT ( 'NONE',  ( -84.59526703719879492, -23.96169478059713498, 10.65365249895717881 ) ) ;
#52846=CARTESIAN_POINT ( 'NONE',  ( -128.5228709571500758, -24.65952944569305316, 1.056160979905707675 ) ) ;
#52847=CARTESIAN_POINT ( 'NONE',  ( -30.60198721217873796, -24.75207560356990300, 8.640809912072075605 ) ) ;
#52848=CARTESIAN_POINT ( 'NONE',  ( 14.64190796094839264, -15.47823801613018269, 11.49999999999998934 ) ) ;
#52849=CARTESIAN_POINT ( 'NONE',  ( -112.5553945339797508, -23.96119346886881729, -0.6495511937831841554 ) ) ;
#52852=CARTESIAN_POINT ( 'NONE',  ( -85.62287095714999907, -24.51254535404255108, 9.355368623467660072 ) ) ;
#52853=B_SPLINE_CURVE_WITH_KNOTS ( 'NONE', 3,
 ( #63588, #70676, #32612, #79781 ),
 .UNSPECIFIED., .F., .F.,
 ( 4, 4 ),
 ( 1.387778780781445521E-17, 9.999999999997510880E-05 ),
 .UNSPECIFIED. ) ;
#52854=CARTESIAN_POINT ( 'NONE',  ( -3.368041826647835357, -22.21310627845187824, -1.500000000000002220 ) ) ;
#52855=EDGE_CURVE ( 'NONE', #85611, #68707, #58413, .T. ) ;
#52856=CARTESIAN_POINT ( 'NONE',  ( -109.9096082921335125, -25.11552134530501590, 2.805129186380272088 ) ) ;
#52857=ORIENTED_EDGE ( 'NONE', *, *, #92599, .F. ) ;
#52858=EDGE_CURVE ( 'NONE', #12032, #26463, #80141, .T. ) ;
#52859=CARTESIAN_POINT ( 'NONE',  ( -81.52287095715004739, -24.35013146730203815, 9.818937971375106599 ) ) ;
#52860=CARTESIAN_POINT ( 'NONE',  ( 18.24213732562919787, -7.162457363581539838, 11.49999999999999645 ) ) ;
#52862=EDGE_CURVE ( 'NONE', #937, #3121, #94123, .T. ) ;
#52863=CARTESIAN_POINT ( 'NONE',  ( -100.6228709571500985, -24.51254535404255464, 9.355368623467651190 ) ) ;
#52864=B_SPLINE_CURVE_WITH_KNOTS ( 'NONE', 3,
 ( #72118, #33044, #17820, #23917, #71614, #40663, #8205, #78196, #1600, #32540, #48787, #39144, #55897, #32037 ),
 .UNSPECIFIED., .F., .F.,
 ( 4, 2, 2, 2, 2, 2, 4 ),
 ( 8.673617379884035472E-19, 0.0001881572706675479123, 0.0003763145413350949572, 0.0007526290826701718083, 0.001128943624005248605, 0.001317100894672787112, 0.001505258165340325402 ),
 .UNSPECIFIED. ) ;
#52865=ORIENTED_EDGE ( 'NONE', *, *, #44741, .F. ) ;
#52867=CARTESIAN_POINT ( 'NONE',  ( -69.20785623293232902, -25.30035436060855503, 5.366416221723499191 ) ) ;
#52870=AXIS2_PLACEMENT_3D ( 'NONE', #55886, #86811, #40652 ) ;
#52872=CARTESIAN_POINT ( 'NONE',  ( -116.6228709571500701, -23.48783264082478794, -1.443836473390058606 ) ) ;
#52874=CARTESIAN_POINT ( 'NONE',  ( 2.169241753049089727, -19.58708112974024829, 11.49999999999998934 ) ) ;
#52875=ORIENTED_EDGE ( 'NONE', *, *, #49972, .T. ) ;
#52876=DIRECTION ( 'NONE',  ( 0.000000000000000000, -0.9999999999976377785, -2.173523156925979552E-06 ) ) ;
#52879=ORIENTED_EDGE ( 'NONE', *, *, #68820, .F. ) ;
#52880=CARTESIAN_POINT ( 'NONE',  ( -45.62287095715004881, -23.47593901973091235, -1.443836447539009749 ) ) ;
#52881=CARTESIAN_POINT ( 'NONE',  ( -67.62287095715007013, -24.51283580621364422, 0.6167428607019762588 ) ) ;
#52882=CARTESIAN_POINT ( 'NONE',  ( -90.62287095715004170, -23.48786465467241058, 11.44779295918254469 ) ) ;
#52884=CARTESIAN_POINT ( 'NONE',  ( -102.6228709571500559, -29.50248528299804818, 1.056150453629042030 ) ) ;
#52886=CARTESIAN_POINT ( 'NONE',  ( -91.52287095715001897, -23.95044443724991368, 10.65354141964648882 ) ) ;
#52887=CARTESIAN_POINT ( 'NONE',  ( 19.98059151383774434, -0.7942727526097331792, -1.500000000000002220 ) ) ;
#52890=CARTESIAN_POINT ( 'NONE',  ( -45.54234093893470003, -24.40133493613049964, 9.663955038902802386 ) ) ;
#52894=B_SPLINE_CURVE_WITH_KNOTS ( 'NONE', 3,
 ( #67503, #74112, #83707, #6587, #45166, #83203, #4609, #74598 ),
 .UNSPECIFIED., .F., .F.,
 ( 4, 2, 2, 4 ),
 ( -0.001224873891641418489, -0.0002244903592271037251, 0.0007758931731872110386, 0.002776660238015837313 ),
 .UNSPECIFIED. ) ;
#52895=B_SPLINE_CURVE_WITH_KNOTS ( 'NONE', 3,
 ( #86187, #16170, #86684, #10560 ),
 .UNSPECIFIED., .F., .F.,
 ( 4, 4 ),
 ( 0.4200858975343448876, 0.4290923288064604213 ),
 .UNSPECIFIED. ) ;
#52896=EDGE_CURVE ( 'NONE', #86931, #89111, #62020, .T. ) ;
#52898=CARTESIAN_POINT ( 'NONE',  ( -80.54557494822695674, -24.52399227489127043, 9.353111116836524630 ) ) ;
#52899=CARTESIAN_POINT ( 'NONE',  ( -125.5798323200307891, -25.21791982601823534, 6.461802024446555492 ) ) ;
#52900=CARTESIAN_POINT ( 'NONE',  ( -39.57598330014963040, -24.65952944569304250, 1.056160979905697017 ) ) ;
#52901=DIRECTION ( 'NONE',  ( 1.000000000000000000, 3.773278334444166432E-23, 8.201307841325785021E-29 ) ) ;
#52905=DIRECTION ( 'NONE',  ( 1.000000000000000000, 3.773278334444166432E-23, 8.201307841325785021E-29 ) ) ;
#52906=VECTOR ( 'NONE', #44189, 1000.000000000000114 ) ;
#52907=EDGE_LOOP ( 'NONE', ( #51909, #66567, #37582, #23450 ) ) ;
#52908=VECTOR ( 'NONE', #6528, 1000.000000000000114 ) ;
#52909=CARTESIAN_POINT ( 'NONE',  ( -3.766600276044322904, -19.90762401167813067, 11.49999999999998934 ) ) ;
#52910=CARTESIAN_POINT ( 'NONE',  ( -69.20005239865344038, -25.31085673378436240, 5.363653916047343984 ) ) ;
#52913=CARTESIAN_POINT ( 'NONE',  ( -35.62287095715005592, -29.50249982740957577, 7.747779886224967605 ) ) ;
#52914=B_SPLINE_CURVE_WITH_KNOTS ( 'NONE', 3,
 ( #42185, #18814, #65528, #35054, #10211, #3610 ),
 .UNSPECIFIED., .F., .F.,
 ( 4, 2, 4 ),
 ( 0.000000000000000000, 0.001380764517854764532, 0.002761529035709529064 ),
 .UNSPECIFIED. ) ;
#52915=EDGE_CURVE ( 'NONE', #77171, #69148, #49980, .T. ) ;
#52918=CARTESIAN_POINT ( 'NONE',  ( -61.62287095715004881, -23.47596703998600631, 11.44779298504227505 ) ) ;
#52919=CARTESIAN_POINT ( 'NONE',  ( 12.55954966114946458, -15.69740789531843461, -1.500000000000002220 ) ) ;
#52920=CARTESIAN_POINT ( 'NONE',  ( 5.245434476726341444, -20.39595507048906242, 11.49999999999999645 ) ) ;
#52921=CARTESIAN_POINT ( 'NONE',  ( -32.52287095715006160, -24.65952944569304606, 1.056160979905690134 ) ) ;
#52922=CARTESIAN_POINT ( 'NONE',  ( 19.10104996495751450, -11.12853483292915691, 11.49999999999998934 ) ) ;
#52924=CARTESIAN_POINT ( 'NONE',  ( -18.81443736134900035, 8.205417114561466718, -1.500000000000002220 ) ) ;
#52925=FACE_OUTER_BOUND ( 'NONE', #35368, .T. ) ;
#52926=CARTESIAN_POINT ( 'NONE',  ( -60.49379600255042533, -24.52300882791528380, 0.6510814631126233820 ) ) ;
#52928=DIRECTION ( 'NONE',  ( -3.773278334453079030E-23, 0.9999999999976377785, 2.173523156925979128E-06 ) ) ;
#52930=CARTESIAN_POINT ( 'NONE',  ( -89.40841769935769889, -25.27880950044345809, 5.947789066509453271 ) ) ;
#52931=CARTESIAN_POINT ( 'NONE',  ( -67.62287095715005592, -24.64965695001468404, 8.947790433994184056 ) ) ;
#52932=VERTEX_POINT ( 'NONE', #64718 ) ;
#52933=B_SPLINE_CURVE_WITH_KNOTS ( 'NONE', 3,
 ( #71513, #40053, #38548, #69504, #30932, #39551 ),
 .UNSPECIFIED., .F., .F.,
 ( 4, 2, 4 ),
 ( 1.570755371633915156E-05, 0.001396183895866087753, 0.002776660238015836446 ),
 .UNSPECIFIED. ) ;
#52934=ORIENTED_EDGE ( 'NONE', *, *, #59655, .T. ) ;
#52936=CARTESIAN_POINT ( 'NONE',  ( -49.64748826666535564, -25.06465475861797998, 7.411158395225631246 ) ) ;
#52937=CARTESIAN_POINT ( 'NONE',  ( -89.62287095715002749, -23.73907113216990794, -1.053371485793227480 ) ) ;
#52938=CARTESIAN_POINT ( 'NONE',  ( -4.647353109605855792, 20.10343637636090719, -1.500000000000002220 ) ) ;
#52939=CARTESIAN_POINT ( 'NONE',  ( 0.6597851148675514255, -21.60297929554585394, 11.49999999999999645 ) ) ;
#52940=VERTEX_POINT ( 'NONE', #50969 ) ;
#52941=DIRECTION ( 'NONE',  ( -3.773278334444167608E-23, 1.000000000000000000, 0.000000000000000000 ) ) ;
#52942=VECTOR ( 'NONE', #56069, 1000.000000000000114 ) ;
#52944=CARTESIAN_POINT ( 'NONE',  ( 22.01400519847025450, -3.885951517071169370, -1.500000000000002220 ) ) ;
#52945=CARTESIAN_POINT ( 'NONE',  ( -93.52287095715006160, -24.64898659630368272, 1.056161002820827921 ) ) ;
#52948=LINE ( 'NONE', #60068, #77637 ) ;
#52949=CARTESIAN_POINT ( 'NONE',  ( -35.57399241795090461, -24.92592662359561118, 8.075495903017992916 ) ) ;
#52951=CARTESIAN_POINT ( 'NONE',  ( -15.12424899162716230, 14.39509690008720177, 11.49999999999998934 ) ) ;
#52952=ORIENTED_EDGE ( 'NONE', *, *, #35904, .F. ) ;
#52953=CARTESIAN_POINT ( 'NONE',  ( -86.54787210963549171, -24.34968618360934300, 0.1864209137778916336 ) ) ;
#52955=ORIENTED_EDGE ( 'NONE', *, *, #11216, .T. ) ;
#52956=CARTESIAN_POINT ( 'NONE',  ( -109.5940830279356248, -23.73791477778912551, 11.05961554403169878 ) ) ;
#52957=CARTESIAN_POINT ( 'NONE',  ( -11.89019930860364482, -17.45089671868802128, -1.500000000000002220 ) ) ;
#52960=CARTESIAN_POINT ( 'NONE',  ( -99.61078991697702634, -25.26221256701134621, 6.818453477056792167 ) ) ;
#52961=CARTESIAN_POINT ( 'NONE',  ( -17.45706314325883213, 13.02611496694466275, 11.49999999999998934 ) ) ;
#52963=CARTESIAN_POINT ( 'NONE',  ( -30.57287095715006231, -23.47596703998576118, 11.44779287168131710 ) ) ;
#52965=CARTESIAN_POINT ( 'NONE',  ( 10.83000837110471082, 18.85367679709202804, -1.500000000000002220 ) ) ;
#52966=CARTESIAN_POINT ( 'NONE',  ( -41.52287095715006870, -24.64898659630528144, 1.056161002820819261 ) ) ;
#52967=CARTESIAN_POINT ( 'NONE',  ( -16.35649155429130985, -15.18990082740072367, 11.49999999999999645 ) ) ;
#52971=CARTESIAN_POINT ( 'NONE',  ( -83.52287095715006160, -23.48786465467241769, 11.44779295918254469 ) ) ;
#52973=AXIS2_PLACEMENT_3D ( 'NONE', #8698, #31521, #70091 ) ;
#52975=ORIENTED_EDGE ( 'NONE', *, *, #68946, .F. ) ;
#52977=CARTESIAN_POINT ( 'NONE',  ( 18.56724428474754518, 10.22298014144217859, -1.500000000000002220 ) ) ;
#52979=CARTESIAN_POINT ( 'NONE',  ( -79.70355613134685768, -25.27791930026442913, 7.365681066972862290 ) ) ;
#52983=CARTESIAN_POINT ( 'NONE',  ( -17.66094656686658482, 7.961706694365092041, 11.49999999999998934 ) ) ;
#52985=CARTESIAN_POINT ( 'NONE',  ( -41.88978735995836189, -25.20650829394578096, 6.812666491500989352 ) ) ;
#52987=AXIS2_PLACEMENT_3D ( 'NONE', #21611, #69804, #45975 ) ;
#52988=EDGE_CURVE ( 'NONE', #62489, #3631, #24443, .T. ) ;
#52989=CARTESIAN_POINT ( 'NONE',  ( 12.19879910451502703, -15.15100395215988449, 11.49999999999999645 ) ) ;
#52991=AXIS2_PLACEMENT_3D ( 'NONE', #64342, #3433, #80034 ) ;
#52994=EDGE_CURVE ( 'NONE', #71801, #89948, #63305, .T. ) ;
#52996=CARTESIAN_POINT ( 'NONE',  ( -44.55620429048338593, -23.47593901973091235, -1.443836447539011525 ) ) ;
#52998=EDGE_CURVE ( 'NONE', #95938, #66032, #3311, .T. ) ;
#52999=CARTESIAN_POINT ( 'NONE',  ( -63.95380932530888884, -23.47596703998600276, 11.44779298504227683 ) ) ;
#53000=CARTESIAN_POINT ( 'NONE',  ( 10.60981200654714307, 16.52409317135366607, -1.500000000000002220 ) ) ;
#53001=EDGE_CURVE ( 'NONE', #56546, #90808, #58444, .T. ) ;
#53003=ORIENTED_EDGE ( 'NONE', *, *, #29948, .F. ) ;
#53004=CARTESIAN_POINT ( 'NONE',  ( 19.31049906410359895, -9.575588319827552652, 11.49999999999998934 ) ) ;
#53007=CARTESIAN_POINT ( 'NONE',  ( -115.6228709571500559, -23.47593901973091235, -1.443836447538997536 ) ) ;
#53009=CARTESIAN_POINT ( 'NONE',  ( -99.99551102217851906, -25.18439353279887527, 3.374614400146649373 ) ) ;
#53010=CARTESIAN_POINT ( 'NONE',  ( -3.381418692465893105, -22.81955385325859709, -1.500000000000002220 ) ) ;
#53013=CARTESIAN_POINT ( 'NONE',  ( -62.62287095715004881, -24.65952944569304606, 1.056160979905693909 ) ) ;
#53014=CARTESIAN_POINT ( 'NONE',  ( -11.96439459519798554, -16.23097265130270728, 11.49999999999999645 ) ) ;
#53015=CARTESIAN_POINT ( 'NONE',  ( -109.0459178056501486, -25.10927576934983563, 3.663605367118155876 ) ) ;
#53017=CARTESIAN_POINT ( 'NONE',  ( -99.62287095715005592, -24.64965695001468404, 8.947790433994178727 ) ) ;
#53019=CARTESIAN_POINT ( 'NONE',  ( -110.5404475696186779, -25.18425585998923921, 3.309296991606290650 ) ) ;
#53020=CARTESIAN_POINT ( 'NONE',  ( -1.769646468872753120, 19.80360307839763934, 11.49999999999998934 ) ) ;
#53021=CARTESIAN_POINT ( 'NONE',  ( -41.55620429048340014, -23.48783264082478084, -1.443836473390071484 ) ) ;
#53022=CARTESIAN_POINT ( 'NONE',  ( 6.953341435731974940, 18.52374150113109152, -1.500000000000002220 ) ) ;
#53023=AXIS2_PLACEMENT_3D ( 'NONE', #11633, #34982, #80158 ) ;
#53025=B_SPLINE_CURVE_WITH_KNOTS ( 'NONE', 3,
 ( #1628, #32559, #23942, #62021 ),
 .UNSPECIFIED., .F., .F.,
 ( 4, 4 ),
 ( 0.000000000000000000, 0.0001002978970083175645 ),
 .UNSPECIFIED. ) ;
#53028=CARTESIAN_POINT ( 'NONE',  ( -18.22997975830956108, -9.740667652671243459, 11.49999999999999645 ) ) ;
#53030=LINE ( 'NONE', #69236, #40240 ) ;
#53033=CARTESIAN_POINT ( 'NONE',  ( -16.51154719052397724, 15.62863258182435189, 11.49999999999999645 ) ) ;
#53037=CARTESIAN_POINT ( 'NONE',  ( 16.36621611169882229, 11.82581248522330064, -1.500000000000002220 ) ) ;
#53038=CARTESIAN_POINT ( 'NONE',  ( -63.64765489167466228, -23.73766607897669090, -1.055555164236456900 ) ) ;
#53039=LINE ( 'NONE', #30175, #57721 ) ;
#53040=ORIENTED_EDGE ( 'NONE', *, *, #16882, .T. ) ;
#53044=CARTESIAN_POINT ( 'NONE',  ( 19.82229641098322404, 11.46754112681587046, 11.49999999999998934 ) ) ;
#53045=CARTESIAN_POINT ( 'NONE',  ( -50.58832339509404363, -25.27420565479429015, 3.304980239963009492 ) ) ;
#53046=CARTESIAN_POINT ( 'NONE',  ( 21.43499300031224664, 3.042053824063517542, -1.500000000000002220 ) ) ;
#53047=CARTESIAN_POINT ( 'NONE',  ( -118.6228709571500559, -29.50250243563736774, 8.947779886222134493 ) ) ;
#53049=CARTESIAN_POINT ( 'NONE',  ( 19.90007246472742608, 6.374896562862660154, 11.49999999999999645 ) ) ;
#53051=CARTESIAN_POINT ( 'NONE',  ( -29.24636659181000198, -25.21267509515801564, 4.940287023516041209 ) ) ;
#53052=CARTESIAN_POINT ( 'NONE',  ( 12.93620265873104991, 17.78788284566447331, 11.49999999999998934 ) ) ;
#53055=CARTESIAN_POINT ( 'NONE',  ( -105.5132737718367650, -24.40133493613049964, 9.663955038902797057 ) ) ;
#53056=CARTESIAN_POINT ( 'NONE',  ( -41.82812249501711932, -25.29087254191939849, 3.843615201987044205 ) ) ;
#53059=EDGE_CURVE ( 'NONE', #66032, #27769, #98303, .T. ) ;
#53060=CARTESIAN_POINT ( 'NONE',  ( -90.54437712527642645, -24.73531770709095312, 8.716586749053512051 ) ) ;
#53061=ORIENTED_EDGE ( 'NONE', *, *, #86469, .F. ) ;
#53065=ORIENTED_EDGE ( 'NONE', *, *, #50462, .F. ) ;
#53066=CARTESIAN_POINT ( 'NONE',  ( -32.52287095715006160, -24.64898659630528854, 1.056161002820817485 ) ) ;
#53067=CARTESIAN_POINT ( 'NONE',  ( -101.6521089408578007, -25.10935970639156523, 3.606142542491853398 ) ) ;
#53068=CARTESIAN_POINT ( 'NONE',  ( -57.49755803318443981, -24.34968618360933590, 0.1864209137778796155 ) ) ;
#53069=B_SPLINE_CURVE_WITH_KNOTS ( 'NONE', 3,
 ( #41776, #49890, #34155, #26539, #57503, #80823 ),
 .UNSPECIFIED., .F., .F.,
 ( 4, 2, 4 ),
 ( 0.000000000000000000, 0.001380764517853252287, 0.002761529035706504574 ),
 .UNSPECIFIED. ) ;
#53070=CARTESIAN_POINT ( 'NONE',  ( 20.11976772532220181, -3.360927329567881205, -1.500000000000002220 ) ) ;
#53073=CARTESIAN_POINT ( 'NONE',  ( -61.22287095715005734, -23.47593901973090169, -1.443836447538997758 ) ) ;
#53074=CARTESIAN_POINT ( 'NONE',  ( -98.58953762381671027, -24.65952944569304606, 1.056160979905695907 ) ) ;
#53075=CARTESIAN_POINT ( 'NONE',  ( -91.52287095715006160, -23.94994826722564341, -0.6494450866342701412 ) ) ;
#53076=ORIENTED_EDGE ( 'NONE', *, *, #47136, .T. ) ;
#53078=CARTESIAN_POINT ( 'NONE',  ( -85.62287095715007013, -25.00158670708909270, 2.256160236439165967 ) ) ;
#53079=B_SPLINE_CURVE_WITH_KNOTS ( 'NONE', 3,
 ( #28282, #29780, #74940, #68350, #52128, #36396, #91669, #82565 ),
 .UNSPECIFIED., .F., .F.,
 ( 4, 2, 2, 4 ),
 ( 6.384118678607358824E-06, 0.002007151183507253651, 0.003007534715921578606, 0.004007918248335903995 ),
 .UNSPECIFIED. ) ;
#53080=CARTESIAN_POINT ( 'NONE',  ( 17.70469293622815243, 10.90570606759641592, 11.49999999999998934 ) ) ;
#53081=ORIENTED_EDGE ( 'NONE', *, *, #1248, .T. ) ;
#53083=EDGE_CURVE ( 'NONE', #8583, #55708, #6304, .T. ) ;
#53086=CARTESIAN_POINT ( 'NONE',  ( -44.52287095715006160, -23.47596703998600631, 11.44779298504229281 ) ) ;
#53087=ORIENTED_EDGE ( 'NONE', *, *, #978, .T. ) ;
#53088=EDGE_LOOP ( 'NONE', ( #99735, #41230, #59680, #16720 ) ) ;
#53090=CARTESIAN_POINT ( 'NONE',  ( -92.62287095715005592, -23.48786465467241413, 11.44779295918254469 ) ) ;
#53093=CARTESIAN_POINT ( 'NONE',  ( -40.62287095715009144, -24.92604778743017491, 8.074972756849357225 ) ) ;
#53094=CARTESIAN_POINT ( 'NONE',  ( -110.5228709571500758, -23.47593901973090524, -1.443836447538996204 ) ) ;
#53095=CARTESIAN_POINT ( 'NONE',  ( -113.6228709571500559, -29.50248528299804818, 1.056150453629043584 ) ) ;
#53096=CARTESIAN_POINT ( 'NONE',  ( -14.81638660137672225, 16.44347145309322045, 11.49999999999999645 ) ) ;
#53097=ORIENTED_EDGE ( 'NONE', *, *, #66447, .T. ) ;
#53099=CARTESIAN_POINT ( 'NONE',  ( 22.61563695565308407, -1.323143620866313208, 11.49999999999998934 ) ) ;
#53100=AXIS2_PLACEMENT_3D ( 'NONE', #94263, #76525, #93260 ) ;
#53101=CARTESIAN_POINT ( 'NONE',  ( -27.83193219186368950, -24.81234328755879659, 7.598342972711060739 ) ) ;
#53102=VERTEX_POINT ( 'NONE', #20491 ) ;
#53103=B_SPLINE_CURVE_WITH_KNOTS ( 'NONE', 3,
 ( #11684, #4595, #86437, #34040 ),
 .UNSPECIFIED., .F., .F.,
 ( 4, 4 ),
 ( 0.6692531030269918135, 0.6702538500677572841 ),
 .UNSPECIFIED. ) ;
#53105=VECTOR ( 'NONE', #24410, 1000.000000000000114 ) ;
#53106=CARTESIAN_POINT ( 'NONE',  ( -99.52287095715006160, -24.65952944569304961, 1.056160979905702346 ) ) ;
#53107=CARTESIAN_POINT ( 'NONE',  ( 4.949566031639514918, 19.51814346981619863, 11.49999999999998934 ) ) ;
#53109=EDGE_LOOP ( 'NONE', ( #71429, #16592, #91376, #24370 ) ) ;
#53111=CARTESIAN_POINT ( 'NONE',  ( 19.81157572017019319, -10.35993776028809421, -1.500000000000002220 ) ) ;
#53112=ORIENTED_EDGE ( 'NONE', *, *, #10282, .T. ) ;
#53113=ORIENTED_EDGE ( 'NONE', *, *, #93615, .F. ) ;
#53114=DIRECTION ( 'NONE',  ( -1.000000000000000000, -3.773278334444167608E-23, -8.201307833595939069E-29 ) ) ;
#53115=CARTESIAN_POINT ( 'NONE',  ( -124.4728709571500360, -25.30558663486635851, 5.000950659935021747 ) ) ;
#53117=CARTESIAN_POINT ( 'NONE',  ( -51.62287095715005592, -29.50247984919015209, -1.443849546365058689 ) ) ;
#53118=CARTESIAN_POINT ( 'NONE',  ( -101.5228709571500900, -24.66019654487200441, 8.947790411086119278 ) ) ;
#53121=CARTESIAN_POINT ( 'NONE',  ( 3.994393897313025743, -19.14333888664780048, 11.49999999999998934 ) ) ;
#53122=EDGE_CURVE ( 'NONE', #88443, #80901, #65641, .T. ) ;
#53123=FACE_OUTER_BOUND ( 'NONE', #59729, .T. ) ;
#53124=CARTESIAN_POINT ( 'NONE',  ( -19.15072323977689095, -9.709862252083167888, -1.500000000000002220 ) ) ;
#53126=EDGE_CURVE ( 'NONE', #63165, #38340, #42634, .T. ) ;
#53127=DIRECTION ( 'NONE',  ( -3.773278334444167608E-23, 1.000000000000000000, 0.000000000000000000 ) ) ;
#53129=CARTESIAN_POINT ( 'NONE',  ( -4.124250913864588419, 22.51598698906299845, -1.500000000000002220 ) ) ;
#53132=CARTESIAN_POINT ( 'NONE',  ( -96.59124853101694441, -24.15620529776628445, 10.23563542870660115 ) ) ;
#53133=CARTESIAN_POINT ( 'NONE',  ( -108.5228709571501327, -23.73907113217652309, -1.053371485781582573 ) ) ;
#53134=CARTESIAN_POINT ( 'NONE',  ( 1.593314845114734535, -19.89410510517485164, 11.49999999999999645 ) ) ;
#53137=CARTESIAN_POINT ( 'NONE',  ( -74.64369162555894377, -23.73791477778911840, 11.05961554403170588 ) ) ;
#53138=CARTESIAN_POINT ( 'NONE',  ( -127.5228709571500332, -24.66019654487200441, 8.947790411086105067 ) ) ;
#53139=ORIENTED_EDGE ( 'NONE', *, *, #76326, .F. ) ;
#53141=CARTESIAN_POINT ( 'NONE',  ( -57.22287095715011418, -23.47593901973090524, -1.443836447538998202 ) ) ;
#53143=CARTESIAN_POINT ( 'NONE',  ( -21.04499429308205549, 5.405531755741471045, 11.49999999999998934 ) ) ;
#53144=DIRECTION ( 'NONE',  ( -3.773278334453079030E-23, 0.9999999999976377785, 2.173523156925979128E-06 ) ) ;
#53145=CARTESIAN_POINT ( 'NONE',  ( 8.161054176536994831, -17.82452852192863091, -1.500000000000002220 ) ) ;
#53147=ORIENTED_EDGE ( 'NONE', *, *, #73256, .F. ) ;
#53151=CARTESIAN_POINT ( 'NONE',  ( -17.91610926057384034, -10.00117247862695358, 11.49999999999999645 ) ) ;
#53152=CARTESIAN_POINT ( 'NONE',  ( -79.52287095715006160, -23.47596703998600631, 11.44779298504228571 ) ) ;
#53153=CARTESIAN_POINT ( 'NONE',  ( -42.58953762381671737, -24.66019654487199375, 8.947790411086133489 ) ) ;
#53154=VERTEX_POINT ( 'NONE', #69169 ) ;
#53156=CARTESIAN_POINT ( 'NONE',  ( -51.52287095715008292, -23.47593901973090169, -1.443836447538997092 ) ) ;
#53158=PLANE ( 'NONE',  #90550 ) ;
#53159=CARTESIAN_POINT ( 'NONE',  ( -104.6228709571500559, -23.47596703998600631, 11.44779298504227860 ) ) ;
#53163=CARTESIAN_POINT ( 'NONE',  ( 7.103900956763240515, -21.94381868531750968, 11.49999999999999645 ) ) ;
#53164=CARTESIAN_POINT ( 'NONE',  ( 4.317061085376620255, -22.40314112565372540, 11.49999999999998934 ) ) ;
#53169=FACE_OUTER_BOUND ( 'NONE', #8367, .T. ) ;
#53170=CARTESIAN_POINT ( 'NONE',  ( -99.60147378138974261, -25.31582203441881163, 4.950471085733717302 ) ) ;
#53171=CARTESIAN_POINT ( 'NONE',  ( -3.478157889954244464, -21.63767827151469447, -1.500000000000002220 ) ) ;
#53175=LINE ( 'NONE', #85105, #47039 ) ;
#53176=CARTESIAN_POINT ( 'NONE',  ( -78.55426290676015810, -23.96119346886880308, -0.6495511937832113558 ) ) ;
#53180=CARTESIAN_POINT ( 'NONE',  ( -1.999887071766271784, 20.33596237858139233, 11.49999999999998934 ) ) ;
#53181=ORIENTED_EDGE ( 'NONE', *, *, #56232, .T. ) ;
#53182=VERTEX_POINT ( 'NONE', #5276 ) ;
#53183=ORIENTED_EDGE ( 'NONE', *, *, #62408, .F. ) ;
#53184=ORIENTED_EDGE ( 'NONE', *, *, #68213, .F. ) ;
#53185=CARTESIAN_POINT ( 'NONE',  ( -18.27982475084466785, -14.08179083545084964, -1.500000000000002220 ) ) ;
#53186=CARTESIAN_POINT ( 'NONE',  ( -95.52287095715006160, -25.00158670708909980, 2.256160236439166411 ) ) ;
#53187=CARTESIAN_POINT ( 'NONE',  ( -10.81679630089563915, -17.07601267366916886, -1.500000000000002220 ) ) ;
#53188=VERTEX_POINT ( 'NONE', #59580 ) ;
#53189=CARTESIAN_POINT ( 'NONE',  ( -122.5228709571500900, -23.94994826722565406, -0.6494450866342689199 ) ) ;
#53191=DIRECTION ( 'NONE',  ( -3.773278334453079618E-23, 0.9999999999976377785, 2.173523156925979975E-06 ) ) ;
#53192=DIRECTION ( 'NONE',  ( -3.773278334444167608E-23, 1.000000000000000000, 0.000000000000000000 ) ) ;
#53193=CARTESIAN_POINT ( 'NONE',  ( -70.50645411744089586, -24.15503026093916006, -0.2815557561904372674 ) ) ;
#53194=CARTESIAN_POINT ( 'NONE',  ( 4.431377227695222132, -20.94745169971119481, 11.49999999999999645 ) ) ;
#53195=VERTEX_POINT ( 'NONE', #67196 ) ;
#53196=CARTESIAN_POINT ( 'NONE',  ( -100.6228709571500559, -23.47593901973091235, -1.443836447539001089 ) ) ;
#53199=CARTESIAN_POINT ( 'NONE',  ( -20.55201672899488585, 2.666056886502145673, -1.500000000000002220 ) ) ;
#53203=ORIENTED_EDGE ( 'NONE', *, *, #32838, .F. ) ;
#53204=CARTESIAN_POINT ( 'NONE',  ( -29.62287095715004881, -24.58457514626677209, 8.947790440257529454 ) ) ;
#53209=CARTESIAN_POINT ( 'NONE',  ( -21.97012646571106842, -0.5360883523215664859, 11.49999999999999645 ) ) ;
#53210=CARTESIAN_POINT ( 'NONE',  ( -91.62287095715004170, -24.65952944569304606, 1.056160979905700792 ) ) ;
#53211=CARTESIAN_POINT ( 'NONE',  ( 14.20245820080859289, -17.52920931871068433, 11.49999999999998934 ) ) ;
#53213=CARTESIAN_POINT ( 'NONE',  ( -15.18370147500227496, -14.46048895944246127, -1.500000000000002220 ) ) ;
#53214=CARTESIAN_POINT ( 'NONE',  ( -109.3584176993576591, -25.28950181196791647, 4.206202504803813191 ) ) ;
#53215=CARTESIAN_POINT ( 'NONE',  ( -30.64535912258471839, -23.53197991584894666, -1.479945482512690313 ) ) ;
#53216=ORIENTED_EDGE ( 'NONE', *, *, #8558, .F. ) ;
#53218=B_SPLINE_CURVE_WITH_KNOTS ( 'NONE', 3,
 ( #65291, #97203, #3380, #58647, #51041, #27202 ),
 .UNSPECIFIED., .F., .F.,
 ( 4, 2, 4 ),
 ( 6.391158118959991367E-06, 0.001387004593080780942, 0.002767618028042601996 ),
 .UNSPECIFIED. ) ;
#53220=VERTEX_POINT ( 'NONE', #14372 ) ;
#53221=CARTESIAN_POINT ( 'NONE',  ( -44.52287095715007581, -24.66019654487199730, 8.947790411086117501 ) ) ;
#53222=CARTESIAN_POINT ( 'NONE',  ( 20.98156868870745484, 4.911575462371418510, -1.500000000000002220 ) ) ;
#53223=CARTESIAN_POINT ( 'NONE',  ( -50.37830952628071657, -25.31401921878212136, 5.197788989978542773 ) ) ;
#53224=EDGE_LOOP ( 'NONE', ( #52759, #84401, #7398, #67325 ) ) ;
#53225=CARTESIAN_POINT ( 'NONE',  ( -15.55823947972799282, -14.28038451723262270, -1.500000000000002220 ) ) ;
#53226=CARTESIAN_POINT ( 'NONE',  ( -67.52287095715003318, -23.47593901973090169, -1.443836447538996870 ) ) ;
#53227=CARTESIAN_POINT ( 'NONE',  ( -81.61611000704996854, -25.24685308744633261, 6.293942982122114671 ) ) ;
#53230=CARTESIAN_POINT ( 'NONE',  ( -42.52287095715005449, -23.47593901973090169, -1.443836447538997092 ) ) ;
#53231=CARTESIAN_POINT ( 'NONE',  ( -0.8134642310582372859, 22.17477653155656725, -1.500000000000002220 ) ) ;
#53232=CARTESIAN_POINT ( 'NONE',  ( -34.62287095715007013, -23.47596703998600276, 11.44779298504227505 ) ) ;
#53233=EDGE_CURVE ( 'NONE', #36594, #12687, #60771, .T. ) ;
#53234=ORIENTED_EDGE ( 'NONE', *, *, #925, .F. ) ;
#53239=CARTESIAN_POINT ( 'NONE',  ( -18.83898130102433299, -4.906684326670742280, 11.49999999999998934 ) ) ;
#53241=CARTESIAN_POINT ( 'NONE',  ( -21.18999663186871274, 2.814949255606389311, 11.49999999999998934 ) ) ;
#53242=CARTESIAN_POINT ( 'NONE',  ( -62.60383260654986515, -23.73766607897669445, -1.055555164236454901 ) ) ;
#53243=DIRECTION ( 'NONE',  ( 0.000000000000000000, -0.9999999999976377785, -2.173523156925979975E-06 ) ) ;
#53244=ADVANCED_FACE ( 'NONE', ( #21978 ), #19036, .T. ) ;
#53245=CARTESIAN_POINT ( 'NONE',  ( -79.62287095715009855, -23.73907113216991860, -1.053371485793228812 ) ) ;
#53246=CARTESIAN_POINT ( 'NONE',  ( -33.62287095715005592, -24.64965695001467694, 8.947790433994189385 ) ) ;
#53247=CARTESIAN_POINT ( 'NONE',  ( -2.225104987405961854, -22.55768739424384606, -1.500000000000002220 ) ) ;
#53248=B_SPLINE_SURFACE_WITH_KNOTS ( 'NONE', 3, 3, ( 
 ( #76007, #84127, #37465, #16113 ),
 ( #85126, #29844, #39462, #69411 ),
 ( #23724, #62309, #93234, #61810 ),
 ( #15612, #84627, #77001, #99832 ),
 ( #91736, #8511, #77503, #898 ),
 ( #8005, #76501, #31853, #38953 ),
 ( #61313, #22710, #69908, #24230 ) ),
 .UNSPECIFIED., .F., .F., .F.,
 ( 4, 3, 4 ),
 ( 4, 4 ),
 ( 0.7945040050992244751, 0.8970133687736505657, 0.9995227324480766562 ),
 ( 0.6896692517579798842, 0.6910003734054406266 ),
 .UNSPECIFIED. ) ;
#53251=DIRECTION ( 'NONE',  ( 3.773278334444166432E-23, -1.000000000000000000, 0.000000000000000000 ) ) ;
#53252=CARTESIAN_POINT ( 'NONE',  ( -19.21288746854601115, 4.878285775029977955, 11.49999999999999645 ) ) ;
#53253=FACE_OUTER_BOUND ( 'NONE', #87897, .T. ) ;
#53254=ORIENTED_EDGE ( 'NONE', *, *, #69062, .F. ) ;
#53257=CARTESIAN_POINT ( 'NONE',  ( -91.15361000704997707, -25.26877915520014639, 5.947789088310639904 ) ) ;
#53258=CARTESIAN_POINT ( 'NONE',  ( 2.186256072416925544, -21.55203199515037582, -1.500000000000002220 ) ) ;
#53259=CARTESIAN_POINT ( 'NONE',  ( -49.19632817692706084, -25.27518035636533966, 3.560433938396965647 ) ) ;
#53261=CARTESIAN_POINT ( 'NONE',  ( 7.440116899146960172, 17.95454168335740874, -1.500000000000002220 ) ) ;
#53262=CARTESIAN_POINT ( 'NONE',  ( -129.6228709571500133, -24.35013146730204525, 9.818937971375103047 ) ) ;
#53263=CARTESIAN_POINT ( 'NONE',  ( -40.55620429048337883, -24.99156044556202261, 7.747789690856173195 ) ) ;
#53264=CARTESIAN_POINT ( 'NONE',  ( -11.05534852661189937, -16.44151763790470966, 11.49999999999998934 ) ) ;
#53266=CARTESIAN_POINT ( 'NONE',  ( 5.353267490507026771, -19.58905154090721368, 11.49999999999999645 ) ) ;
#53267=CARTESIAN_POINT ( 'NONE',  ( -80.58318732538134554, -24.83618233451450408, 1.606449574219532384 ) ) ;
#53269=ORIENTED_EDGE ( 'NONE', *, *, #36573, .T. ) ;
#53270=CARTESIAN_POINT ( 'NONE',  ( -102.5148950863152493, -24.15620529776628800, 10.23563542870660292 ) ) ;
#53271=CARTESIAN_POINT ( 'NONE',  ( -78.62287095715005592, -29.50250243563736774, 8.947779886222141599 ) ) ;
#53272=FACE_OUTER_BOUND ( 'NONE', #90505, .T. ) ;
#53274=FACE_OUTER_BOUND ( 'NONE', #7706, .T. ) ;
#53275=FACE_OUTER_BOUND ( 'NONE', #364, .T. ) ;
#53276=CARTESIAN_POINT ( 'NONE',  ( -14.83682921977595548, 13.52632505182701017, -1.500000000000002220 ) ) ;
#53277=CARTESIAN_POINT ( 'NONE',  ( -85.52287095715009002, -23.47593901973090524, -1.443836447538996648 ) ) ;
#53278=VERTEX_POINT ( 'NONE', #40227 ) ;
#53279=CARTESIAN_POINT ( 'NONE',  ( -129.5562042904834072, -23.47593901973091235, -1.443836447538995760 ) ) ;
#53280=B_SPLINE_CURVE_WITH_KNOTS ( 'NONE', 3,
 ( #86057, #100252, #70842, #1334, #32268, #18546 ),
 .UNSPECIFIED., .F., .F.,
 ( 4, 2, 4 ),
 ( 6.391158118973929294E-06, 0.001387004593080793302, 0.002767618028042612404 ),
 .UNSPECIFIED. ) ;
#53281=CARTESIAN_POINT ( 'NONE',  ( 5.768980952343642166, -22.17701263744951490, 11.49999999999999645 ) ) ;
#53282=CARTESIAN_POINT ( 'NONE',  ( -21.73129956901698989, 6.668506094012985663, -1.500000000000002220 ) ) ;
#53283=CARTESIAN_POINT ( 'NONE',  ( 5.514125806255895004E-17, -29.50250786944455328, 11.44777956126000618 ) ) ;
#53285=CARTESIAN_POINT ( 'NONE',  ( -39.66885951848129821, -25.23677723931214700, 3.617518980680364038 ) ) ;
#53286=CARTESIAN_POINT ( 'NONE',  ( -89.58953762381671027, -23.47593901973091235, -1.443836447539002865 ) ) ;
#53287=CARTESIAN_POINT ( 'NONE',  ( -118.6228709571500559, -24.66019654487200086, 8.947790411086117501 ) ) ;
#53289=EDGE_CURVE ( 'NONE', #53154, #90318, #53959, .T. ) ;
#53291=ORIENTED_EDGE ( 'NONE', *, *, #80942, .F. ) ;
#53292=CARTESIAN_POINT ( 'NONE',  ( -19.47531982339030776, -5.969937916086089480, 11.49999999999998934 ) ) ;
#53293=VERTEX_POINT ( 'NONE', #70170 ) ;
#53294=CARTESIAN_POINT ( 'NONE',  ( 19.50756536182865020, -12.10693203178887423, -1.500000000000002220 ) ) ;
#53299=B_SPLINE_CURVE_WITH_KNOTS ( 'NONE', 3,
 ( #62738, #23640, #62232, #7423 ),
 .UNSPECIFIED., .F., .F.,
 ( 4, 4 ),
 ( 0.9111506303623450043, 0.9201570616344605380 ),
 .UNSPECIFIED. ) ;
#53300=CARTESIAN_POINT ( 'NONE',  ( -40.62287095715005592, -23.47593901973091235, -1.443836447539011525 ) ) ;
#53301=CARTESIAN_POINT ( 'NONE',  ( 3.248270302591931724, 20.98854991013365279, 11.49999999999999645 ) ) ;
#53304=CARTESIAN_POINT ( 'NONE',  ( 12.10043277420606778, 18.60588626676543100, -1.500000000000002220 ) ) ;
#53305=CARTESIAN_POINT ( 'NONE',  ( -19.87711886888390822, 5.503898473480427711, 11.49999999999998934 ) ) ;
#53306=ADVANCED_FACE ( 'NONE', ( #2179 ), #43391, .T. ) ;
#53307=VERTEX_POINT ( 'NONE', #655 ) ;
#53309=CARTESIAN_POINT ( 'NONE',  ( -109.2582164645601779, -25.27682770776893051, 5.068133765414451375 ) ) ;
#53311=CARTESIAN_POINT ( 'NONE',  ( -39.18285704424624782, -25.23459596353552215, 3.598380491417637383 ) ) ;
#53315=ADVANCED_FACE ( 'NONE', ( #71681 ), #39211, .T. ) ;
#53316=AXIS2_PLACEMENT_3D ( 'NONE', #44815, #67164, #13343 ) ;
#53318=B_SPLINE_CURVE_WITH_KNOTS ( 'NONE', 3,
 ( #50339, #34615, #4161, #27503, #42249, #89890 ),
 .UNSPECIFIED., .F., .F.,
 ( 4, 2, 4 ),
 ( 1.570887131794333942E-05, 0.001396322306279758904, 0.002776935741241574537 ),
 .UNSPECIFIED. ) ;
#53319=CARTESIAN_POINT ( 'NONE',  ( -127.4728709570019589, -25.30556169000782418, 4.803960565675224892 ) ) ;
#53320=CARTESIAN_POINT ( 'NONE',  ( -106.5228709571500900, -23.47593901973090524, -1.443836447538996204 ) ) ;
#53321=CARTESIAN_POINT ( 'NONE',  ( 20.34438994040483806, -4.565235006643893811, -1.500000000000002220 ) ) ;
#53322=CARTESIAN_POINT ( 'NONE',  ( -3.058130702743298901, -21.54894043062209263, 11.49999999999999645 ) ) ;
#53323=CARTESIAN_POINT ( 'NONE',  ( -51.91874251014689179, -25.22891536400416967, 6.366542672068985276 ) ) ;
#53324=CARTESIAN_POINT ( 'NONE',  ( -78.55878950404671457, -23.73791477778911840, 11.05961554403170588 ) ) ;
#53325=CARTESIAN_POINT ( 'NONE',  ( -12.88509029660790617, -18.40938060607246740, 11.49999999999998934 ) ) ;
#53326=EDGE_CURVE ( 'NONE', #84514, #69684, #7767, .T. ) ;
#53328=ADVANCED_FACE ( 'NONE', ( #23984 ), #45054, .T. ) ;
#53331=CARTESIAN_POINT ( 'NONE',  ( -50.52287095715006870, -24.52323809116984776, 9.355190652339430812 ) ) ;
#53332=CARTESIAN_POINT ( 'NONE',  ( -96.52287095715001897, -24.66019654487199730, 8.947790411086115725 ) ) ;
#53333=ADVANCED_FACE ( 'NONE', ( #65093 ), #4668, .T. ) ;
#53337=CARTESIAN_POINT ( 'NONE',  ( -46.59984483897366658, -23.96169478059712432, 10.65365249895718414 ) ) ;
#53339=CARTESIAN_POINT ( 'NONE',  ( 21.32124590881793225, -1.116183810207903804, -1.500000000000002220 ) ) ;
#53340=VERTEX_POINT ( 'NONE', #35118 ) ;
#53341=CARTESIAN_POINT ( 'NONE',  ( -5.295558097854481616, 20.35707381486366785, 11.49999999999998934 ) ) ;
#53342=CARTESIAN_POINT ( 'NONE',  ( -30.57663643993555525, -23.78769947764003234, -0.9707498849204322378 ) ) ;
#53344=CARTESIAN_POINT ( 'NONE',  ( -113.5228709571500332, -23.95044443724993144, 10.65354141964649415 ) ) ;
#53345=B_SPLINE_CURVE_WITH_KNOTS ( 'NONE', 3,
 ( #94710, #25698, #26204, #2885, #48562, #25193 ),
 .UNSPECIFIED., .F., .F.,
 ( 4, 2, 4 ),
 ( 1.570887131794638196E-05, 0.001396322306279760422, 0.002776935741241574537 ),
 .UNSPECIFIED. ) ;
#53346=DIRECTION ( 'NONE',  ( -3.773278334453079030E-23, 0.9999999999976377785, 2.173523156925979128E-06 ) ) ;
#53347=CARTESIAN_POINT ( 'NONE',  ( 17.71009474140864981, 13.04663522181963309, -1.500000000000002220 ) ) ;
#53348=CARTESIAN_POINT ( 'NONE',  ( -87.62602669543169043, -24.51314013834317151, 0.6176544820404251679 ) ) ;
#53349=VERTEX_POINT ( 'NONE', #43235 ) ;
#53350=CARTESIAN_POINT ( 'NONE',  ( -30.64751926837171325, -23.47596703998600631, 11.44779298504228038 ) ) ;
#53351=EDGE_CURVE ( 'NONE', #20842, #81045, #2730, .T. ) ;
#53352=CARTESIAN_POINT ( 'NONE',  ( -84.58830421338662120, -24.35071581493543391, 9.817618358456027039 ) ) ;
#53353=CARTESIAN_POINT ( 'NONE',  ( -130.5728709571500588, -24.37807914296825729, 0.3010598746230642719 ) ) ;
#53354=CARTESIAN_POINT ( 'NONE',  ( -10.29676400380902734, -22.20978366736605381, 10.97511746239722008 ) ) ;
#53355=CARTESIAN_POINT ( 'NONE',  ( 17.78463046036513617, -11.72987588014745342, -1.500000000000002220 ) ) ;
#53356=DIRECTION ( 'NONE',  ( 3.773278334444167608E-23, -1.000000000000000000, 0.000000000000000000 ) ) ;
#53357=CARTESIAN_POINT ( 'NONE',  ( -107.5489731280372467, -24.66019654487199730, 8.947790411086115725 ) ) ;
#53358=B_SPLINE_CURVE_WITH_KNOTS ( 'NONE', 3,
 ( #96429, #81705, #57888, #88826 ),
 .UNSPECIFIED., .F., .F.,
 ( 4, 4 ),
 ( 1.387778780781445676E-17, 0.0001000000000000028508 ),
 .UNSPECIFIED. ) ;
#53361=CARTESIAN_POINT ( 'NONE',  ( -33.53192614058710319, -24.51314013834315375, 0.6176544820404119562 ) ) ;
#53362=CARTESIAN_POINT ( 'NONE',  ( -14.31525571501011207, 17.33968770572689166, -1.500000000000002220 ) ) ;
#53363=EDGE_CURVE ( 'NONE', #59077, #68398, #78900, .T. ) ;
#53364=CARTESIAN_POINT ( 'NONE',  ( -109.9084783329273023, -25.25626643526282322, 3.571638612575483318 ) ) ;
#53366=CARTESIAN_POINT ( 'NONE',  ( -99.05911678666235787, -25.18602439098982870, 6.775663951083587655 ) ) ;
#53367=CARTESIAN_POINT ( 'NONE',  ( -18.74126595726828626, 5.813943427813767606, 11.49999999999999645 ) ) ;
#53368=CARTESIAN_POINT ( 'NONE',  ( -28.62287095715003460, -23.80623360916731102, -0.6494981922848278577 ) ) ;
#53372=CARTESIAN_POINT ( 'NONE',  ( -88.51439832242913042, -23.96169478059713853, 10.65365249895717703 ) ) ;
#53373=CARTESIAN_POINT ( 'NONE',  ( -125.2171600754302716, -25.33572514627022798, 6.311475924823946926 ) ) ;
#53374=CARTESIAN_POINT ( 'NONE',  ( -89.90493557854645701, -25.06732983082694588, 7.447789526168958396 ) ) ;
#53377=CARTESIAN_POINT ( 'NONE',  ( -18.24397684793207830, 7.494555614300850266, -1.500000000000002220 ) ) ;
#53379=VERTEX_POINT ( 'NONE', #36108 ) ;
#53381=LINE ( 'NONE', #14294, #56113 ) ;
#53383=EDGE_LOOP ( 'NONE', ( #27870, #86629, #39339, #19729 ) ) ;
#53387=CARTESIAN_POINT ( 'NONE',  ( -100.0332803147414324, -25.26638532029810946, 7.519340188766448385 ) ) ;
#53390=CARTESIAN_POINT ( 'NONE',  ( -69.88050735872322150, -25.31201612363421916, 5.413835025572902637 ) ) ;
#53391=CARTESIAN_POINT ( 'NONE',  ( -112.5228709571500616, -24.64898659630529210, 1.056161002820831474 ) ) ;
#53392=CARTESIAN_POINT ( 'NONE',  ( 13.87436705529610492, 14.39054836566213780, -1.500000000000002220 ) ) ;
#53394=CARTESIAN_POINT ( 'NONE',  ( -45.61117613609256694, -23.85049219812685450, 10.88485053497527133 ) ) ;
#53396=B_SPLINE_CURVE_WITH_KNOTS ( 'NONE', 3,
 ( #78464, #77460, #70878, #7960, #69869, #63278 ),
 .UNSPECIFIED., .F., .F.,
 ( 4, 2, 4 ),
 ( 0.000000000000000000, 0.001380901958385396351, 0.002761803916770792702 ),
 .UNSPECIFIED. ) ;
#53398=B_SPLINE_CURVE_WITH_KNOTS ( 'NONE', 3,
 ( #31728, #93609, #41344, #55076 ),
 .UNSPECIFIED., .F., .F.,
 ( 4, 4 ),
 ( 6.938893903907228378E-18, 9.999999999999591193E-05 ),
 .UNSPECIFIED. ) ;
#53403=CARTESIAN_POINT ( 'NONE',  ( -81.58232796345568261, -24.65952944569304961, 1.056160979905703901 ) ) ;
#53408=FACE_OUTER_BOUND ( 'NONE', #24617, .T. ) ;
#53410=CARTESIAN_POINT ( 'NONE',  ( -20.02346298389695534, -3.155783441878276196, 11.49999999999998934 ) ) ;
#53411=CARTESIAN_POINT ( 'NONE',  ( -61.52287095715006870, -24.50216790748205398, 0.6166512839542451774 ) ) ;
#53412=CARTESIAN_POINT ( 'NONE',  ( -49.62287095715004170, -23.96127896941632685, -0.6493128931037893681 ) ) ;
#53413=CARTESIAN_POINT ( 'NONE',  ( -39.52287095715006870, -23.47593901973090524, -1.443836447538997092 ) ) ;
#53414=ORIENTED_EDGE ( 'NONE', *, *, #80012, .F. ) ;
#53417=CARTESIAN_POINT ( 'NONE',  ( 19.99232773509726258, 2.034096180923423702, -1.500000000000002220 ) ) ;
#53418=CARTESIAN_POINT ( 'NONE',  ( 19.39439428382967634, -8.317090367284466268, 11.49999999999999645 ) ) ;
#53419=CARTESIAN_POINT ( 'NONE',  ( -101.5228709571500332, -23.94994826722564696, -0.6494450866342716955 ) ) ;
#53420=CARTESIAN_POINT ( 'NONE',  ( 20.57361055066190758, -8.084994430987380909, 11.49999999999998934 ) ) ;
#53421=CARTESIAN_POINT ( 'NONE',  ( 20.53815866822273861, -0.6333348845813139283, 11.49999999999998934 ) ) ;
#53422=CARTESIAN_POINT ( 'NONE',  ( -32.07722060962682775, -29.50250091417111520, 8.247779886223803203 ) ) ;
#53423=B_SPLINE_CURVE_WITH_KNOTS ( 'NONE', 3,
 ( #44726, #28001, #59452, #75651 ),
 .UNSPECIFIED., .F., .F.,
 ( 4, 4 ),
 ( 0.2489393459054682345, 0.2499400929462335941 ),
 .UNSPECIFIED. ) ;
#53425=CARTESIAN_POINT ( 'NONE',  ( -60.53568055955854277, -24.73486907724917572, 1.287355809206962576 ) ) ;
#53426=ORIENTED_EDGE ( 'NONE', *, *, #98031, .T. ) ;
#53427=LINE ( 'NONE', #59543, #15252 ) ;
#53428=VERTEX_POINT ( 'NONE', #37605 ) ;
#53430=B_SPLINE_SURFACE_WITH_KNOTS ( 'NONE', 3, 1, ( 
 ( #89527, #19010 ),
 ( #11407, #81420 ),
 ( #18513, #96150 ),
 ( #66220, #58584 ),
 ( #19510, #65226 ),
 ( #41360, #87536 ),
 ( #18016, #3809 ),
 ( #71818, #80416 ),
 ( #25630, #2307 ),
 ( #41873, #10910 ),
 ( #50471, #49487 ),
 ( #88535, #95144 ),
 ( #34746, #65719 ),
 ( #73313, #2810 ),
 ( #64218, #26637 ),
 ( #3320, #81915 ),
 ( #72313, #33747 ),
 ( #33238, #72817 ),
 ( #48979, #34251 ) ),
 .UNSPECIFIED., .F., .F., .F.,
 ( 4, 1, 1, 1, 1, 1, 1, 1, 1, 1, 1, 1, 1, 1, 1, 1, 4 ),
 ( 2, 2 ),
 ( 0.000000000000000000, 0.07126869258656032269, 0.1398117850281277164, 0.2064974320993705204, 0.2715352442755388784, 0.3360818306156446722, 0.4005283877476332743, 0.4649838426509124156, 0.5300503053616137938, 0.5944234089533948495, 0.6555827099825238813, 0.7148491056365311458, 0.7721150638705993607, 0.8289992113006462437, 0.8851221627752358101, 0.9420793532637975476, 1.000000000000000000 ),
 ( 0.000000000000000000, 1.000000000000000000 ),
 .UNSPECIFIED. ) ;
#53431=CARTESIAN_POINT ( 'NONE',  ( -67.62287095715007013, -23.72773821059536559, 11.05748984161097681 ) ) ;
#53432=ORIENTED_EDGE ( 'NONE', *, *, #67809, .T. ) ;
#53433=EDGE_LOOP ( 'NONE', ( #6995, #35340, #56380, #35982 ) ) ;
#53434=ORIENTED_EDGE ( 'NONE', *, *, #39104, .T. ) ;
#53435=CARTESIAN_POINT ( 'NONE',  ( -80.88924702628075636, -25.29868576439400840, 4.592921234843194256 ) ) ;
#53438=CARTESIAN_POINT ( 'NONE',  ( 16.46467569749531634, 12.45148609503053017, -1.500000000000002220 ) ) ;
#53439=B_SPLINE_CURVE_WITH_KNOTS ( 'NONE', 3,
 ( #30526, #1089, #31024, #31524, #22396, #62490, #77183, #54880 ),
 .UNSPECIFIED., .F., .F.,
 ( 4, 2, 2, 4 ),
 ( 6.391158118973815792E-06, 0.002007136338672934825, 0.003007508928949912969, 0.004007881519226891114 ),
 .UNSPECIFIED. ) ;
#53440=CARTESIAN_POINT ( 'NONE',  ( -10.14273968512601520, 19.10955606681249463, 11.49999999999999645 ) ) ;
#53441=VERTEX_POINT ( 'NONE', #5651 ) ;
#53442=LINE ( 'NONE', #47324, #6170 ) ;
#53443=CARTESIAN_POINT ( 'NONE',  ( -57.62287095715004881, -23.72773821059535138, 11.05748984161097503 ) ) ;
#53444=CARTESIAN_POINT ( 'NONE',  ( -22.37156870845955225, 0.5457896250522937809, 11.49999999999998934 ) ) ;
#53445=EDGE_CURVE ( 'NONE', #58220, #80787, #39013, .T. ) ;
#53447=CARTESIAN_POINT ( 'NONE',  ( -80.15527233487838998, -25.27875081312351213, 7.057877889425411055 ) ) ;
#53449=ORIENTED_EDGE ( 'NONE', *, *, #15754, .F. ) ;
#53451=CARTESIAN_POINT ( 'NONE',  ( -49.53128083207727173, -24.66019654487198665, 8.947790411086131712 ) ) ;
#53453=CARTESIAN_POINT ( 'NONE',  ( -33.52287095715006160, -24.64898659630367206, 1.056161002820817485 ) ) ;
#53454=CARTESIAN_POINT ( 'NONE',  ( 12.70736309587848645, -16.60074808024427284, -1.500000000000002220 ) ) ;
#53455=VERTEX_POINT ( 'NONE', #21363 ) ;
#53457=CARTESIAN_POINT ( 'NONE',  ( -67.55938062934993127, -23.73791477778911840, 11.05961554403170766 ) ) ;
#53459=ORIENTED_EDGE ( 'NONE', *, *, #74950, .T. ) ;
#53460=CARTESIAN_POINT ( 'NONE',  ( -109.5961252891390956, -23.48786465467241769, 11.44779295918253759 ) ) ;
#53461=CARTESIAN_POINT ( 'NONE',  ( -1.756177585742932479, 21.11346882147791959, -1.500000000000002220 ) ) ;
#53462=ORIENTED_EDGE ( 'NONE', *, *, #73876, .F. ) ;
#53463=CARTESIAN_POINT ( 'NONE',  ( -122.6228709571500417, -23.47596703998600631, 11.44779298504227860 ) ) ;
#53464=DIRECTION ( 'NONE',  ( 0.000000000000000000, -0.9999999999976377785, -2.173523156925979975E-06 ) ) ;
#53465=CARTESIAN_POINT ( 'NONE',  ( -5.167225684058948332, 21.16526716281445530, 11.49999999999998934 ) ) ;
#53466=CARTESIAN_POINT ( 'NONE',  ( -37.92287095715006728, -23.47596703998600276, 11.44779298504227683 ) ) ;
#53468=CARTESIAN_POINT ( 'NONE',  ( -35.62287095715005592, -24.99156045073392463, 7.747789690856161648 ) ) ;
#53470=CARTESIAN_POINT ( 'NONE',  ( -9.754611696910345131, 19.53525426502628548, -1.500000000000002220 ) ) ;
#53471=CARTESIAN_POINT ( 'NONE',  ( -71.44479781437794941, -25.31639555109142492, 5.279211600726748443 ) ) ;
#53472=CARTESIAN_POINT ( 'NONE',  ( 1.165341552704713513, 22.26021350444069213, 11.49999999999999645 ) ) ;
#53473=VERTEX_POINT ( 'NONE', #82280 ) ;
#53475=CARTESIAN_POINT ( 'NONE',  ( -74.52287095715007581, -24.64898659630528854, 1.056161002820824368 ) ) ;
#53478=ORIENTED_EDGE ( 'NONE', *, *, #39779, .T. ) ;
#53479=ORIENTED_EDGE ( 'NONE', *, *, #28265, .T. ) ;
#53482=ORIENTED_EDGE ( 'NONE', *, *, #32659, .F. ) ;
#53486=CARTESIAN_POINT ( 'NONE',  ( -16.84575021678815432, -12.90291372800108505, -1.500000000000002220 ) ) ;
#53487=CARTESIAN_POINT ( 'NONE',  ( -94.63061204461861564, -24.15543982623907482, -0.2315651400026595141 ) ) ;
#53488=CARTESIAN_POINT ( 'NONE',  ( -95.62287095715001328, -24.14406661707766943, 10.28769366152059206 ) ) ;
#53492=AXIS2_PLACEMENT_3D ( 'NONE', #77780, #30623, #61603 ) ;
#53493=CARTESIAN_POINT ( 'NONE',  ( -37.62287095715004170, -24.35013146730202394, 9.818937971375111928 ) ) ;
#53494=CARTESIAN_POINT ( 'NONE',  ( -70.04794951447323115, -25.31059997604261369, 5.351382493944067953 ) ) ;
#53495=ORIENTED_EDGE ( 'NONE', *, *, #49336, .F. ) ;
#53496=CARTESIAN_POINT ( 'NONE',  ( -1.307668758097810358, 19.38731951181482671, 11.49999999999999645 ) ) ;
#53498=VERTEX_POINT ( 'NONE', #60464 ) ;
#53500=FACE_OUTER_BOUND ( 'NONE', #30249, .T. ) ;
#53502=EDGE_CURVE ( 'NONE', #32461, #91753, #30555, .T. ) ;
#53503=B_SPLINE_CURVE_WITH_KNOTS ( 'NONE', 3,
 ( #19400, #4191, #98512, #5675, #83293, #20891 ),
 .UNSPECIFIED., .F., .F.,
 ( 4, 2, 4 ),
 ( 0.000000000000000000, 0.001380901958385384858, 0.002761803916770769717 ),
 .UNSPECIFIED. ) ;
#53504=CARTESIAN_POINT ( 'NONE',  ( -110.6228709571500843, -23.47596703998600631, 11.44779298504227860 ) ) ;
#53505=CARTESIAN_POINT ( 'NONE',  ( -18.14765110722914798, -7.448729197826248871, 11.49999999999998934 ) ) ;
#53506=CARTESIAN_POINT ( 'NONE',  ( -41.15947890742572923, -25.27806083308631102, 4.822226191762938541 ) ) ;
#53507=ORIENTED_EDGE ( 'NONE', *, *, #76331, .T. ) ;
#53508=CARTESIAN_POINT ( 'NONE',  ( 20.98369277809155165, -4.918611649023987731, -1.500000000000002220 ) ) ;
#53509=CARTESIAN_POINT ( 'NONE',  ( -33.64272694203721414, -24.15620529776627379, 10.23563542870661536 ) ) ;
#53512=DIRECTION ( 'NONE',  ( 3.773278334444166432E-23, -1.000000000000000000, 0.000000000000000000 ) ) ;
#53513=CARTESIAN_POINT ( 'NONE',  ( 19.44587849558928738, -12.39355811350142922, -1.500000000000002220 ) ) ;
#53515=CARTESIAN_POINT ( 'NONE',  ( -93.60099715520429697, -23.48783264082477018, -1.443836473390090580 ) ) ;
#53516=DIRECTION ( 'NONE',  ( -3.773278334453079618E-23, 0.9999999999976377785, 2.173523156925979975E-06 ) ) ;
#53517=CARTESIAN_POINT ( 'NONE',  ( 10.87751022112437482, 17.06716278085755079, 11.49999999999999645 ) ) ;
#53518=CARTESIAN_POINT ( 'NONE',  ( -121.6252487271805904, -24.15620529776628445, 10.23563542870660115 ) ) ;
#53520=CARTESIAN_POINT ( 'NONE',  ( -110.6079876523469920, -25.29823816284334015, 2.855977437720611523 ) ) ;
#53522=CARTESIAN_POINT ( 'NONE',  ( -111.1213521864704035, -25.18425657249500205, 3.637108438862380222 ) ) ;
#53523=CARTESIAN_POINT ( 'NONE',  ( 14.98761344906185577, -13.09354923471379983, -1.500000000000002220 ) ) ;
#53525=CARTESIAN_POINT ( 'NONE',  ( -18.77405512783484198, 6.205181830411797606, -1.500000000000002220 ) ) ;
#53526=CARTESIAN_POINT ( 'NONE',  ( -56.58745316763238264, -24.34968618360933590, 0.1864209137778786995 ) ) ;
#53527=CARTESIAN_POINT ( 'NONE',  ( -108.5562042904833930, -24.64898659630528854, 1.056161002820831474 ) ) ;
#53529=CARTESIAN_POINT ( 'NONE',  ( -6.067718162532647064, 19.77315050736717694, 11.49999999999999645 ) ) ;
#53530=CARTESIAN_POINT ( 'NONE',  ( -98.55620429048339304, -24.64898659630529210, 1.056161002820829253 ) ) ;
#53531=VECTOR ( 'NONE', #74392, 1000.000000000000114 ) ;
#53532=CARTESIAN_POINT ( 'NONE',  ( -106.5970357503859134, -23.48783264082477729, -1.443836473390085695 ) ) ;
#53533=CARTESIAN_POINT ( 'NONE',  ( -4.508144621425604903, 22.28865971958312997, 11.49999999999999645 ) ) ;
#53534=VERTEX_POINT ( 'NONE', #35933 ) ;
#53535=CARTESIAN_POINT ( 'NONE',  ( -65.62287095715005592, -23.47596703998600631, 11.44779298504227683 ) ) ;
#53537=CARTESIAN_POINT ( 'NONE',  ( 18.63370447891095694, 7.782165041754079304, -1.500000000000002220 ) ) ;
#53539=CARTESIAN_POINT ( 'NONE',  ( -52.62287095715005592, -23.47593901973091235, -1.443836447539009749 ) ) ;
#53540=ORIENTED_EDGE ( 'NONE', *, *, #100288, .F. ) ;
#53543=CARTESIAN_POINT ( 'NONE',  ( -4.124250913864588419, 22.51598698906299845, -1.500000000000002220 ) ) ;
#53544=CARTESIAN_POINT ( 'NONE',  ( -50.67443072449054853, -25.27420569099243153, 3.321634375823972807 ) ) ;
#53546=CARTESIAN_POINT ( 'NONE',  ( -1.126084586642228436, -21.63456646517454729, -1.500000000000002220 ) ) ;
#53547=FACE_OUTER_BOUND ( 'NONE', #57194, .T. ) ;
#53548=CARTESIAN_POINT ( 'NONE',  ( -34.56115368636444174, -23.73766607897670866, -1.055555164236443133 ) ) ;
#53549=CARTESIAN_POINT ( 'NONE',  ( -15.06743543786183714, 14.52697759824333090, 11.49999999999999645 ) ) ;
#53550=ORIENTED_EDGE ( 'NONE', *, *, #24836, .F. ) ;
#53553=CARTESIAN_POINT ( 'NONE',  ( -7.037580251249667462, -20.86201633182841420, 11.49999999999998934 ) ) ;
#53554=B_SPLINE_CURVE_WITH_KNOTS ( 'NONE', 3,
 ( #3077, #99750, #62228, #39376 ),
 .UNSPECIFIED., .F., .F.,
 ( 4, 4 ),
 ( 0.000000000000000000, 9.999999999998897304E-05 ),
 .UNSPECIFIED. ) ;
#53555=AXIS2_PLACEMENT_3D ( 'NONE', #91662, #83044, #37886 ) ;
#53557=CARTESIAN_POINT ( 'NONE',  ( -40.62732473945732181, -25.10925769753297132, 2.839336373176108097 ) ) ;
#53560=CARTESIAN_POINT ( 'NONE',  ( -109.8650237084402619, -25.29042187987247914, 5.784623108531866897 ) ) ;
#53561=AXIS2_PLACEMENT_3D ( 'NONE', #94214, #2385, #70387 ) ;
#53562=VERTEX_POINT ( 'NONE', #28319 ) ;
#53563=CARTESIAN_POINT ( 'NONE',  ( -72.52211241193376168, -23.48786465467241058, 11.44779295918254824 ) ) ;
#53565=ORIENTED_EDGE ( 'NONE', *, *, #51413, .T. ) ;
#53567=ORIENTED_EDGE ( 'NONE', *, *, #983, .T. ) ;
#53568=CARTESIAN_POINT ( 'NONE',  ( -106.6228709571500559, -23.48783264082479150, -1.443836473390060382 ) ) ;
#53569=CARTESIAN_POINT ( 'NONE',  ( -117.6228709571500559, -24.64965695001469115, 8.947790433994175174 ) ) ;
#53571=CARTESIAN_POINT ( 'NONE',  ( 9.418145840992488971, -18.15903486995133065, -1.500000000000002220 ) ) ;
#53572=EDGE_CURVE ( 'NONE', #77786, #11989, #11165, .T. ) ;
#53577=CARTESIAN_POINT ( 'NONE',  ( -0.5504121640580519337, 22.28327991085032878, 11.49999999999998934 ) ) ;
#53579=DIRECTION ( 'NONE',  ( 0.000000000000000000, 0.9999999999976377785, 2.173523156925979975E-06 ) ) ;
#53582=CARTESIAN_POINT ( 'NONE',  ( -29.72101455834852146, -25.16604849282684953, 3.657981149200824067 ) ) ;
#53583=CARTESIAN_POINT ( 'NONE',  ( -28.79021057664958505, -25.26248001664178489, 7.906027797108415633 ) ) ;
#53584=CARTESIAN_POINT ( 'NONE',  ( 20.60118427460899326, -2.865472796819775958, 11.49999999999998934 ) ) ;
#53585=VERTEX_POINT ( 'NONE', #49681 ) ;
#53586=DIRECTION ( 'NONE',  ( -3.773278334453079618E-23, 0.9999999999976377785, 2.173523156925979975E-06 ) ) ;
#53587=ORIENTED_EDGE ( 'NONE', *, *, #25437, .T. ) ;
#53588=CARTESIAN_POINT ( 'NONE',  ( -50.45832920465950622, -25.12217862368817833, 7.100425717848583673 ) ) ;
#53589=EDGE_CURVE ( 'NONE', #73517, #65188, #81440, .T. ) ;
#53590=VERTEX_POINT ( 'NONE', #12086 ) ;
#53595=LINE ( 'NONE', #785, #48570 ) ;
#53596=CARTESIAN_POINT ( 'NONE',  ( -92.52216712986863456, -23.48786465467241413, 11.44779295918254469 ) ) ;
#53597=CARTESIAN_POINT ( 'NONE',  ( -73.52287095715007581, -24.66019654487199730, 8.947790411086121054 ) ) ;
#53598=CARTESIAN_POINT ( 'NONE',  ( -18.17467834739497690, 12.62983929299386965, 11.49999999999999645 ) ) ;
#53600=B_SPLINE_CURVE_WITH_KNOTS ( 'NONE', 3,
 ( #81614, #34443, #19201, #27327 ),
 .UNSPECIFIED., .F., .F.,
 ( 4, 4 ),
 ( 0.000000000000000000, 9.999999999997510880E-05 ),
 .UNSPECIFIED. ) ;
#53602=CARTESIAN_POINT ( 'NONE',  ( -4.753580043990282888, 22.13494492317406070, -1.500000000000002220 ) ) ;
#53603=B_SPLINE_CURVE_WITH_KNOTS ( 'NONE', 3,
 ( #46275, #595, #78700, #77202 ),
 .UNSPECIFIED., .F., .F.,
 ( 4, 4 ),
 ( 0.4290738132432640461, 0.4300745602840295723 ),
 .UNSPECIFIED. ) ;
#53604=CARTESIAN_POINT ( 'NONE',  ( -28.04500620809958633, -24.83830431419368168, 7.554707623994477927 ) ) ;
#53607=CARTESIAN_POINT ( 'NONE',  ( -57.52287095715005449, -23.47596703998600631, 11.44779298504228926 ) ) ;
#53608=AXIS2_PLACEMENT_3D ( 'NONE', #36726, #42858, #91003 ) ;
#53609=CARTESIAN_POINT ( 'NONE',  ( 10.61947033613929214, 17.11087026910869469, 11.49999999999998934 ) ) ;
#53610=CARTESIAN_POINT ( 'NONE',  ( -80.62287095715007013, -25.00158670708909625, 2.256160236439165967 ) ) ;
#53613=CARTESIAN_POINT ( 'NONE',  ( -22.12323335113916301, -3.008119206214963981, -1.500000000000002220 ) ) ;
#53614=ORIENTED_EDGE ( 'NONE', *, *, #96654, .T. ) ;
#53615=ORIENTED_EDGE ( 'NONE', *, *, #34681, .T. ) ;
#53617=CARTESIAN_POINT ( 'NONE',  ( -81.17863363258938136, -25.06437624333259251, 7.413012740375775955 ) ) ;
#53621=CARTESIAN_POINT ( 'NONE',  ( -80.52287095715006160, -24.99156044556202616, 7.747789690856173195 ) ) ;
#53623=CARTESIAN_POINT ( 'NONE',  ( 16.94836550497923966, -9.742303593519430649, 11.49999999999998934 ) ) ;
#53624=FACE_OUTER_BOUND ( 'NONE', #13284, .T. ) ;
#53626=CARTESIAN_POINT ( 'NONE',  ( -21.39523464106120088, -1.845724655749456433, -1.500000000000002220 ) ) ;
#53627=CARTESIAN_POINT ( 'NONE',  ( -25.54641640974780259, -24.92775264709239735, 4.381685759940232572 ) ) ;
#53628=CARTESIAN_POINT ( 'NONE',  ( -99.52287095715006160, -24.64898659630529565, 1.056161002820829697 ) ) ;
#53629=FACE_OUTER_BOUND ( 'NONE', #43211, .T. ) ;
#53631=CARTESIAN_POINT ( 'NONE',  ( 5.898633191892585614, -22.09092271590295198, -1.500000000000002220 ) ) ;
#53634=DIRECTION ( 'NONE',  ( -3.773278334453079618E-23, 0.9999999999976377785, 2.173523156925978705E-06 ) ) ;
#53635=CARTESIAN_POINT ( 'NONE',  ( -17.55682386033230102, 9.526633247210019917, 11.49999999999999645 ) ) ;
#53637=CARTESIAN_POINT ( 'NONE',  ( -63.52287095715006160, -29.50247984919015209, -1.443849546365056913 ) ) ;
#53641=FACE_OUTER_BOUND ( 'NONE', #99351, .T. ) ;
#53643=CARTESIAN_POINT ( 'NONE',  ( 12.24854465327799424, 17.96525243877979605, 11.49999999999998934 ) ) ;
#53644=CARTESIAN_POINT ( 'NONE',  ( -117.5562042904833930, -23.48783264082479150, -1.443836473390057717 ) ) ;
#53645=CARTESIAN_POINT ( 'NONE',  ( -17.52035102510334141, -8.822347199899118309, -1.500000000000002220 ) ) ;
#53646=CARTESIAN_POINT ( 'NONE',  ( -85.52287095715009002, -24.15516710230293995, 10.28746687063725673 ) ) ;
#53647=PLANE ( 'NONE',  #71020 ) ;
#53649=CARTESIAN_POINT ( 'NONE',  ( -91.52216439397189163, -23.48786465467241413, 11.44779295918254469 ) ) ;
#53651=CARTESIAN_POINT ( 'NONE',  ( 10.70087849588422380, -17.49211976490306597, 11.49999999999999645 ) ) ;
#53654=ORIENTED_EDGE ( 'NONE', *, *, #44099, .F. ) ;
#53656=CARTESIAN_POINT ( 'NONE',  ( -109.5689024885030136, -25.30516380716661473, 4.853503604351335987 ) ) ;
#53657=CARTESIAN_POINT ( 'NONE',  ( -39.74201634257447324, -25.18430928084150722, 3.555062059022910503 ) ) ;
#53658=CARTESIAN_POINT ( 'NONE',  ( -108.6228709571500701, -23.48783264082478794, -1.443836473390060604 ) ) ;
#53660=CARTESIAN_POINT ( 'NONE',  ( -123.5228709571500616, -23.47596703998600631, 11.44779298504227860 ) ) ;
#53661=CARTESIAN_POINT ( 'NONE',  ( -119.6228709571501412, -23.73907113216991860, -1.053371485793221707 ) ) ;
#53663=CARTESIAN_POINT ( 'NONE',  ( -20.21456430084473155, -11.12997698910670152, 11.49999999999999645 ) ) ;
#53664=CARTESIAN_POINT ( 'NONE',  ( 13.80103769381473811, 18.14473668730428813, 11.49999999999998934 ) ) ;
#53667=CARTESIAN_POINT ( 'NONE',  ( -86.52287095715007581, -23.72773821059536914, 11.05748984161097503 ) ) ;
#53668=CARTESIAN_POINT ( 'NONE',  ( -13.02831144489870319, 18.26546089674541307, 11.49999999999999645 ) ) ;
#53669=CARTESIAN_POINT ( 'NONE',  ( -94.62287095715005592, -23.48786465467241769, 11.44779295918254114 ) ) ;
#53672=CARTESIAN_POINT ( 'NONE',  ( -21.90371867972833542, 1.011951690471867060, 11.49999999999998934 ) ) ;
#53676=CARTESIAN_POINT ( 'NONE',  ( -78.64223654750129811, -23.73766607897670511, -1.055555164236459342 ) ) ;
#53677=DIRECTION ( 'NONE',  ( -3.773278334453080206E-23, 0.9999999999976377785, 2.173523156925979975E-06 ) ) ;
#53678=VERTEX_POINT ( 'NONE', #74004 ) ;
#53679=EDGE_CURVE ( 'NONE', #24333, #84073, #76559, .T. ) ;
#53680=CARTESIAN_POINT ( 'NONE',  ( -13.28352777634190396, 15.58691228024164310, -1.500000000000002220 ) ) ;
#53682=ORIENTED_EDGE ( 'NONE', *, *, #90154, .F. ) ;
#53684=ORIENTED_EDGE ( 'NONE', *, *, #49399, .F. ) ;
#53685=CARTESIAN_POINT ( 'NONE',  ( -18.27982475084466785, -14.08179083545084964, 11.49999999999998934 ) ) ;
#53686=CARTESIAN_POINT ( 'NONE',  ( -61.51536558186042214, -23.73766607897670156, -1.055555164236459342 ) ) ;
#53687=CARTESIAN_POINT ( 'NONE',  ( -19.34540493331696354, 6.066486871809979142, -1.500000000000002220 ) ) ;
#53688=EDGE_CURVE ( 'NONE', #86907, #94697, #53600, .T. ) ;
#53689=ORIENTED_EDGE ( 'NONE', *, *, #52029, .F. ) ;
#53690=CARTESIAN_POINT ( 'NONE',  ( -122.5228709571500758, -24.50216790748203977, 0.6166512839542626079 ) ) ;
#53691=CARTESIAN_POINT ( 'NONE',  ( -87.62287095715008434, -23.96177878511309345, 10.65340807706329862 ) ) ;
#53692=EDGE_CURVE ( 'NONE', #67691, #67908, #43874, .T. ) ;
#53693=AXIS2_PLACEMENT_3D ( 'NONE', #72349, #73836, #20048 ) ;
#53694=LINE ( 'NONE', #29839, #39976 ) ;
#53695=CARTESIAN_POINT ( 'NONE',  ( -70.65896196779819149, -23.48783264082477018, -1.443836473390095021 ) ) ;
#53696=CARTESIAN_POINT ( 'NONE',  ( -21.38522110535750542, 1.317000383210971792, 11.49999999999999645 ) ) ;
#53698=CARTESIAN_POINT ( 'NONE',  ( -113.6228709571500559, -24.64898659630368627, 1.056161002820831474 ) ) ;
#53700=EDGE_CURVE ( 'NONE', #74034, #30069, #7361, .T. ) ;
#53701=ORIENTED_EDGE ( 'NONE', *, *, #80354, .F. ) ;
#53703=CARTESIAN_POINT ( 'NONE',  ( 20.67342648114324533, -1.018679444107209342, 11.49999999999998934 ) ) ;
#53705=CARTESIAN_POINT ( 'NONE',  ( -123.6228709571501270, -24.34917612406838217, 0.1852690917426666195 ) ) ;
#53706=ORIENTED_EDGE ( 'NONE', *, *, #88650, .T. ) ;
#53707=CARTESIAN_POINT ( 'NONE',  ( -68.52287095715006160, -29.50250786944525672, 11.44777988621623699 ) ) ;
#53708=ORIENTED_EDGE ( 'NONE', *, *, #60213, .F. ) ;
#53711=ADVANCED_FACE ( 'NONE', ( #30308 ), #45554, .T. ) ;
#53712=CARTESIAN_POINT ( 'NONE',  ( -76.52287095715011844, -23.73934037231757088, 11.05740245334328975 ) ) ;
#53713=CARTESIAN_POINT ( 'NONE',  ( -10.95654650054425794, 19.06054500580150446, 11.49999999999999645 ) ) ;
#53714=LINE ( 'NONE', #45595, #23623 ) ;
#53715=CARTESIAN_POINT ( 'NONE',  ( -0.2110286175373513040, -22.56517410205234597, -1.500000000000002220 ) ) ;
#53716=CARTESIAN_POINT ( 'NONE',  ( -20.44905293368100985, -4.654758753755802836, 11.49999999999998934 ) ) ;
#53719=ORIENTED_EDGE ( 'NONE', *, *, #85917, .F. ) ;
#53720=VERTEX_POINT ( 'NONE', #53669 ) ;
#53721=ORIENTED_EDGE ( 'NONE', *, *, #52297, .T. ) ;
#53722=CARTESIAN_POINT ( 'NONE',  ( -36.62287095715007013, -23.73907113216990084, -1.053371485793234363 ) ) ;
#53723=CARTESIAN_POINT ( 'NONE',  ( -7.189238790567602067, -20.27908067168375794, -1.500000000000002220 ) ) ;
#53726=CARTESIAN_POINT ( 'NONE',  ( 5.126256225908648823, -20.47799061884807870, -1.500000000000002220 ) ) ;
#53728=CARTESIAN_POINT ( 'NONE',  ( -129.9395376238166762, -23.47593901973090524, -1.443836447538995982 ) ) ;
#53729=CARTESIAN_POINT ( 'NONE',  ( -64.58953762381672448, -23.48783264082478084, -1.443836473390069042 ) ) ;
#53730=CARTESIAN_POINT ( 'NONE',  ( -118.6228709571500559, -23.47593901973091235, -1.443836447538997536 ) ) ;
#53731=LINE ( 'NONE', #83158, #87583 ) ;
#53732=CARTESIAN_POINT ( 'NONE',  ( -4.315754209668272168, 21.71352930684897942, -1.500000000000002220 ) ) ;
#53733=B_SPLINE_CURVE_WITH_KNOTS ( 'NONE', 3,
 ( #93932, #41675, #72618, #3115 ),
 .UNSPECIFIED., .F., .F.,
 ( 4, 4 ),
 ( 0.000000000000000000, 0.0001000000000000098033 ),
 .UNSPECIFIED. ) ;
#53734=CARTESIAN_POINT ( 'NONE',  ( -71.52210976968737555, -23.48783264082477018, -1.443836473390092578 ) ) ;
#53737=CARTESIAN_POINT ( 'NONE',  ( -51.60144572864662393, -25.24860078279246167, 5.335378098060613361 ) ) ;
#53738=DIRECTION ( 'NONE',  ( -3.773278334453079618E-23, 0.9999999999976377785, 2.173523156925979975E-06 ) ) ;
#53739=CARTESIAN_POINT ( 'NONE',  ( -126.5215136065718298, -23.96119346886880663, -0.6495511937832031402 ) ) ;
#53740=EDGE_CURVE ( 'NONE', #69290, #100338, #91210, .T. ) ;
#53742=CARTESIAN_POINT ( 'NONE',  ( 19.04819733361787470, -3.913502273677552878, 11.49999999999998934 ) ) ;
#53743=CARTESIAN_POINT ( 'NONE',  ( 16.24497012180664868, 13.92215130028523973, 11.49999999999998934 ) ) ;
#53745=CARTESIAN_POINT ( 'NONE',  ( -106.5895376238167387, -23.48783264082479150, -1.443836473390060382 ) ) ;
#53746=VECTOR ( 'NONE', #31787, 1000.000000000000114 ) ;
#53747=CARTESIAN_POINT ( 'NONE',  ( -109.9161100070499515, -25.05712135967894838, 7.447789548357302891 ) ) ;
#53748=CARTESIAN_POINT ( 'NONE',  ( -44.52287095715006160, -23.47596703998600631, 11.44779298504229281 ) ) ;
#53749=CARTESIAN_POINT ( 'NONE',  ( 22.47986593085892437, -3.190245585651162230, -1.500000000000002220 ) ) ;
#53750=B_SPLINE_CURVE_WITH_KNOTS ( 'NONE', 3,
 ( #62680, #762, #39319, #25090, #77371, #17486 ),
 .UNSPECIFIED., .F., .F.,
 ( 4, 2, 4 ),
 ( 1.570887131795109485E-05, 0.001396322306279764325, 0.002776935741241577573 ),
 .UNSPECIFIED. ) ;
#53751=EDGE_CURVE ( 'NONE', #62185, #65047, #49813, .T. ) ;
#53752=CARTESIAN_POINT ( 'NONE',  ( -98.59947353796640357, -23.48783264082476308, -1.443836473390089914 ) ) ;
#53753=CARTESIAN_POINT ( 'NONE',  ( -57.62287095715004881, -23.48786465467241058, 11.44779295918254824 ) ) ;
#53754=CARTESIAN_POINT ( 'NONE',  ( 10.49454761162020588, -16.79419365751139637, 11.49999999999999645 ) ) ;
#53756=ORIENTED_EDGE ( 'NONE', *, *, #99470, .F. ) ;
#53757=EDGE_CURVE ( 'NONE', #16349, #94877, #99386, .T. ) ;
#53758=CARTESIAN_POINT ( 'NONE',  ( -53.62287095715008434, -23.95044443724990657, 10.65354141964650125 ) ) ;
#53759=DIRECTION ( 'NONE',  ( 0.000000000000000000, -0.9999999999976377785, -2.173523156925979128E-06 ) ) ;
#53760=CARTESIAN_POINT ( 'NONE',  ( 21.02075834227166951, -5.193550065563941942, -1.500000000000002220 ) ) ;
#53762=CARTESIAN_POINT ( 'NONE',  ( 19.02374887324148389, -3.781047496429098764, -1.500000000000002220 ) ) ;
#53765=CARTESIAN_POINT ( 'NONE',  ( -0.3680779360730609406, 19.82951397037014729, -1.500000000000002220 ) ) ;
#53767=VERTEX_POINT ( 'NONE', #59787 ) ;
#53769=CARTESIAN_POINT ( 'NONE',  ( 19.83649001621966335, 4.521578618930774951, 11.49999999999999645 ) ) ;
#53770=DIRECTION ( 'NONE',  ( 3.773278334444166432E-23, -1.000000000000000000, 0.000000000000000000 ) ) ;
#53773=EDGE_LOOP ( 'NONE', ( #79718, #72534, #24072, #78224 ) ) ;
#53774=CARTESIAN_POINT ( 'NONE',  ( -102.6269066921069850, -24.35071581493543391, 9.817618358456027039 ) ) ;
#53775=CARTESIAN_POINT ( 'NONE',  ( -92.62287095715005592, -29.50248528299804818, 1.056150453629040253 ) ) ;
#53777=CARTESIAN_POINT ( 'NONE',  ( -40.55012497585009612, -24.15602025860895097, 10.28564288303536856 ) ) ;
#53779=CARTESIAN_POINT ( 'NONE',  ( -9.072532997253766496, -17.89392090870456542, 11.49999999999998934 ) ) ;
#53780=CARTESIAN_POINT ( 'NONE',  ( -120.5562042904833930, -25.00182538069145721, 7.747789668545100206 ) ) ;
#53781=VERTEX_POINT ( 'NONE', #13079 ) ;
#53782=CARTESIAN_POINT ( 'NONE',  ( -97.26334014122947735, -23.56000036390796737, 11.50200000000000067 ) ) ;
#53783=CARTESIAN_POINT ( 'NONE',  ( -6.237877366497927234, -22.00199818733190327, 11.49999999999999645 ) ) ;
#53784=CARTESIAN_POINT ( 'NONE',  ( -17.66434017299383896, 14.31182286555179139, 11.49999999999998934 ) ) ;
#53785=ORIENTED_EDGE ( 'NONE', *, *, #86604, .F. ) ;
#53788=CARTESIAN_POINT ( 'NONE',  ( -38.49806573675382282, -24.15620529776627379, 10.23563542870660825 ) ) ;
#53789=FACE_OUTER_BOUND ( 'NONE', #70166, .T. ) ;
#53790=CARTESIAN_POINT ( 'NONE',  ( -128.5213301548511708, -24.66019654487200441, 8.947790411086112172 ) ) ;
#53792=CARTESIAN_POINT ( 'NONE',  ( -84.52287095715006160, -24.64898659630528854, 1.056161002820826145 ) ) ;
#53793=VERTEX_POINT ( 'NONE', #99801 ) ;
#53794=CARTESIAN_POINT ( 'NONE',  ( 19.78452974690265975, -4.759501717958375622, 11.49999999999998934 ) ) ;
#53795=ORIENTED_EDGE ( 'NONE', *, *, #67075, .F. ) ;
#53796=EDGE_CURVE ( 'NONE', #72922, #73446, #75473, .T. ) ;
#53797=CARTESIAN_POINT ( 'NONE',  ( 9.898807498884217182, 20.75630955806377287, -1.500000000000002220 ) ) ;
#53798=CARTESIAN_POINT ( 'NONE',  ( -37.52287095715006870, -24.65952944569304250, 1.056160979905691910 ) ) ;
#53800=CARTESIAN_POINT ( 'NONE',  ( -38.62287095715005592, -24.64898659630528144, 1.056161002820819261 ) ) ;
#53801=CARTESIAN_POINT ( 'NONE',  ( -77.63398783460891650, -24.15620529776628800, 10.23563542870659937 ) ) ;
#53803=CARTESIAN_POINT ( 'NONE',  ( 4.979423480801214552, 20.69870207611912605, 11.49999999999999645 ) ) ;
#53804=ORIENTED_EDGE ( 'NONE', *, *, #52348, .T. ) ;
#53805=EDGE_CURVE ( 'NONE', #61182, #41839, #41359, .T. ) ;
#53806=ORIENTED_EDGE ( 'NONE', *, *, #26561, .T. ) ;
#53807=CARTESIAN_POINT ( 'NONE',  ( 19.10802705166043580, 11.29804532628753044, 11.49999999999998934 ) ) ;
#53809=ADVANCED_FACE ( 'NONE', ( #84600 ), #83090, .F. ) ;
#53810=CARTESIAN_POINT ( 'NONE',  ( 4.765357849511589805, 20.07956653139741121, -1.500000000000002220 ) ) ;
#53813=CARTESIAN_POINT ( 'NONE',  ( -109.7388188129343831, -25.31627439868620399, 5.649347606066585037 ) ) ;
#53815=EDGE_LOOP ( 'NONE', ( #46914, #41380, #92492, #35457 ) ) ;
#53816=B_SPLINE_CURVE_WITH_KNOTS ( 'NONE', 3,
 ( #18299, #50752, #25406, #72594, #96421, #12169, #94915, #41648 ),
 .UNSPECIFIED., .F., .F.,
 ( 4, 2, 2, 4 ),
 ( -0.001224554619866357556, -0.0002241820295893757250, 0.0007761905606876061056, 0.002776935741241574971 ),
 .UNSPECIFIED. ) ;
#53817=CARTESIAN_POINT ( 'NONE',  ( -91.55174515373460054, -24.15543982623907482, -0.2315651400026614848 ) ) ;
#53819=CARTESIAN_POINT ( 'NONE',  ( -35.62287095715004881, -23.48783264082477729, -1.443836473390072372 ) ) ;
#53820=CARTESIAN_POINT ( 'NONE',  ( -88.55620429048337883, -24.66019654487199730, 8.947790411086126383 ) ) ;
#53821=CARTESIAN_POINT ( 'NONE',  ( -12.81329989551134751, 16.42372500408851366, -1.500000000000002220 ) ) ;
#53822=ADVANCED_FACE ( 'NONE', ( #53169 ), #51667, .T. ) ;
#53823=CARTESIAN_POINT ( 'NONE',  ( 9.899741330608472722, -19.37759744025533593, 11.49999999999999645 ) ) ;
#53824=CARTESIAN_POINT ( 'NONE',  ( -102.6228709571500985, -24.35013146730205236, 9.818937971375103047 ) ) ;
#53826=CARTESIAN_POINT ( 'NONE',  ( -78.59205417243056502, -24.15620529776628445, 10.23563542870660292 ) ) ;
#53827=CARTESIAN_POINT ( 'NONE',  ( 22.29217321540274099, 2.676729263222305644, 11.49999999999998934 ) ) ;
#53828=CARTESIAN_POINT ( 'NONE',  ( -118.5922148814283332, -23.73791477778912551, 11.05961554403169878 ) ) ;
#53829=ORIENTED_EDGE ( 'NONE', *, *, #52203, .F. ) ;
#53832=CARTESIAN_POINT ( 'NONE',  ( -57.62287095715003460, -24.65952944569304606, 1.056160979905696573 ) ) ;
#53835=ORIENTED_EDGE ( 'NONE', *, *, #41255, .T. ) ;
#53836=B_SPLINE_CURVE_WITH_KNOTS ( 'NONE', 3,
 ( #39971, #33354, #64343, #62835, #56720, #80035 ),
 .UNSPECIFIED., .F., .F.,
 ( 4, 2, 4 ),
 ( 0.000000000000000000, 0.001380764517854765182, 0.002761529035709530365 ),
 .UNSPECIFIED. ) ;
#53837=ORIENTED_EDGE ( 'NONE', *, *, #10527, .T. ) ;
#53838=CARTESIAN_POINT ( 'NONE',  ( -21.04715019690976874, -3.721878931196799467, -1.500000000000002220 ) ) ;
#53839=ORIENTED_EDGE ( 'NONE', *, *, #89628, .T. ) ;
#53840=CARTESIAN_POINT ( 'NONE',  ( 18.24537196375281312, 10.48796402029766739, 11.49999999999998934 ) ) ;
#53841=CARTESIAN_POINT ( 'NONE',  ( -30.51841394749799719, -23.78320206874146692, -0.9707498849204322378 ) ) ;
#53842=CARTESIAN_POINT ( 'NONE',  ( -111.3646597888658079, -25.28962345428254466, 4.196480316672507094 ) ) ;
#53844=CARTESIAN_POINT ( 'NONE',  ( 13.70243205411677145, -17.22335469805116048, -1.500000000000002220 ) ) ;
#53845=DIRECTION ( 'NONE',  ( 1.000000000000000000, 3.773278334444166432E-23, 8.201307841325785021E-29 ) ) ;
#53847=LINE ( 'NONE', #78153, #51875 ) ;
#53848=CARTESIAN_POINT ( 'NONE',  ( -107.6228709571500701, -23.47593901973091235, -1.443836447538999312 ) ) ;
#53851=CARTESIAN_POINT ( 'NONE',  ( -130.5728709571500588, -24.47827083238277623, 0.5637492489085987879 ) ) ;
#53852=CARTESIAN_POINT ( 'NONE',  ( -10.24009726630766792, -23.09230492046942373, 8.909134979017293787 ) ) ;
#53853=CARTESIAN_POINT ( 'NONE',  ( 18.63368790978032763, -10.32677859091227113, 11.49999999999998934 ) ) ;
#53854=CARTESIAN_POINT ( 'NONE',  ( -31.24388727629349205, -25.15755375362809332, 2.812131853976373108 ) ) ;
#53857=CARTESIAN_POINT ( 'NONE',  ( -109.5228709571500616, -29.50250243563736774, 8.947779886222136270 ) ) ;
#53858=PLANE ( 'NONE',  #96213 ) ;
#53859=CARTESIAN_POINT ( 'NONE',  ( 20.54305097139451064, 9.177977666691313985, -1.500000000000002220 ) ) ;
#53860=EDGE_CURVE ( 'NONE', #47188, #25509, #30378, .T. ) ;
#53861=VECTOR ( 'NONE', #71326, 1000.000000000000114 ) ;
#53864=CARTESIAN_POINT ( 'NONE',  ( -51.46125951134513343, -25.28644161259768453, 5.846423438430858432 ) ) ;
#53865=CARTESIAN_POINT ( 'NONE',  ( 2.166912399371504705, 19.51343182558466793, 11.49999999999999645 ) ) ;
#53866=CARTESIAN_POINT ( 'NONE',  ( -28.62287095715006302, -23.33147402473456822, -1.443835808584760683 ) ) ;
#53867=CARTESIAN_POINT ( 'NONE',  ( -100.6228709571500843, -23.84081130438200802, 10.88220057463249191 ) ) ;
#53868=ORIENTED_EDGE ( 'NONE', *, *, #79834, .T. ) ;
#53869=CARTESIAN_POINT ( 'NONE',  ( -88.59844203645263860, -23.73791477778912196, 11.05961554403170588 ) ) ;
#53870=CARTESIAN_POINT ( 'NONE',  ( -127.4728709572982268, -25.40561138053049461, 5.197941002177326908 ) ) ;
#53871=CARTESIAN_POINT ( 'NONE',  ( -90.93238060386713073, -25.32379766982192848, 4.367815445636563432 ) ) ;
#53872=CARTESIAN_POINT ( 'NONE',  ( -14.12090166725071327, 13.77431136191591143, 11.49999999999998934 ) ) ;
#53873=ORIENTED_EDGE ( 'NONE', *, *, #30517, .F. ) ;
#53876=CARTESIAN_POINT ( 'NONE',  ( -38.62287095715005592, -23.48783264082477373, -1.443836473390072594 ) ) ;
#53881=CARTESIAN_POINT ( 'NONE',  ( -124.5228709571500900, -24.33927499327855770, 9.819080762295802955 ) ) ;
#53882=CARTESIAN_POINT ( 'NONE',  ( -107.6228709571500701, -23.73907113216991860, -1.053371485793223261 ) ) ;
#53884=CARTESIAN_POINT ( 'NONE',  ( -66.52287095715004739, -23.94994826722564696, -0.6494450866342730277 ) ) ;
#53885=CARTESIAN_POINT ( 'NONE',  ( -67.62287095715005592, -23.72747288104442021, -1.053458166803662666 ) ) ;
#53886=CARTESIAN_POINT ( 'NONE',  ( -123.9228709571500531, -23.47593901973090524, -1.443836447538996426 ) ) ;
#53888=CARTESIAN_POINT ( 'NONE',  ( 12.72590371223024697, 15.41468647733915809, -1.500000000000002220 ) ) ;
#53889=CARTESIAN_POINT ( 'NONE',  ( -100.0924861708260636, -25.27532869707566832, 2.869718512938838728 ) ) ;
#53890=CARTESIAN_POINT ( 'NONE',  ( -51.62026654418801996, -25.30014445700734882, 4.382141121099416559 ) ) ;
#53891=ORIENTED_EDGE ( 'NONE', *, *, #22037, .F. ) ;
#53893=EDGE_CURVE ( 'NONE', #70110, #29423, #12212, .T. ) ;
#53896=CARTESIAN_POINT ( 'NONE',  ( -119.5556275160544004, -23.96119346886881019, -0.6495511937832018079 ) ) ;
#53897=CARTESIAN_POINT ( 'NONE',  ( -110.1380102904055178, -25.18430157207432529, 3.309553953209654065 ) ) ;
#53899=CARTESIAN_POINT ( 'NONE',  ( -106.6228709571500559, -23.48786465467241769, 11.44779295918253759 ) ) ;
#53900=FACE_OUTER_BOUND ( 'NONE', #43373, .T. ) ;
#53901=CARTESIAN_POINT ( 'NONE',  ( -83.60404438967992746, -23.48783264082477018, -1.443836473390093911 ) ) ;
#53902=B_SPLINE_CURVE_WITH_KNOTS ( 'NONE', 3,
 ( #90869, #21340, #19846, #67548 ),
 .UNSPECIFIED., .F., .F.,
 ( 4, 4 ),
 ( 0.000000000000000000, 0.0001000000000000306200 ),
 .UNSPECIFIED. ) ;
#53903=CARTESIAN_POINT ( 'NONE',  ( -66.62287095715005592, -29.50248528299804818, 1.056150453629036701 ) ) ;
#53905=CARTESIAN_POINT ( 'NONE',  ( -55.62287095715004170, -24.99156045073392463, 7.747789690856161648 ) ) ;
#53907=CARTESIAN_POINT ( 'NONE',  ( 3.949161919925879172, -19.86910077469890723, -1.500000000000002220 ) ) ;
#53908=VECTOR ( 'NONE', #17522, 1000.000000000000114 ) ;
#53909=ADVANCED_FACE ( 'NONE', ( #57371, #11659 ), #29645, .T. ) ;
#53910=CARTESIAN_POINT ( 'NONE',  ( -61.52287095715005449, -23.72747288104469732, -1.053458166803227458 ) ) ;
#53911=DIRECTION ( 'NONE',  ( 1.000000000000000000, 3.773278334444167608E-23, 8.201307833595939069E-29 ) ) ;
#53913=ORIENTED_EDGE ( 'NONE', *, *, #78278, .T. ) ;
#53914=DIRECTION ( 'NONE',  ( 0.000000000000000000, 2.173523156925980399E-06, -0.9999999999976378895 ) ) ;
#53915=CARTESIAN_POINT ( 'NONE',  ( 20.11291949428234105, -1.170665973999911902, -1.500000000000002220 ) ) ;
#53916=CARTESIAN_POINT ( 'NONE',  ( 20.91448408463407205, 2.778442817847782020, 11.49999999999999645 ) ) ;
#53918=CARTESIAN_POINT ( 'NONE',  ( 21.13397978930849064, -6.478279476769641221, 11.49999999999998934 ) ) ;
#53919=ADVANCED_FACE ( 'NONE', ( #35010 ), #14243, .T. ) ;
#53920=CARTESIAN_POINT ( 'NONE',  ( 19.85418835109896563, -5.301297255791479479, 11.49999999999998934 ) ) ;
#53922=VECTOR ( 'NONE', #43137, 1000.000000000000114 ) ;
#53923=CARTESIAN_POINT ( 'NONE',  ( -60.52202397238360732, -23.48783264082477018, -1.443836473390097908 ) ) ;
#53924=ORIENTED_EDGE ( 'NONE', *, *, #83125, .F. ) ;
#53925=PLANE ( 'NONE',  #41193 ) ;
#53926=ORIENTED_EDGE ( 'NONE', *, *, #1955, .T. ) ;
#53928=CARTESIAN_POINT ( 'NONE',  ( -51.62287095715005592, -23.47593901973091235, -1.443836447539009749 ) ) ;
#53929=CARTESIAN_POINT ( 'NONE',  ( -67.62287095715001328, -24.33927499327853639, 9.819080762295815390 ) ) ;
#53933=DIRECTION ( 'NONE',  ( 1.000000000000000000, 3.773278334444167608E-23, 8.201307833595939069E-29 ) ) ;
#53934=FACE_OUTER_BOUND ( 'NONE', #25511, .T. ) ;
#53935=CARTESIAN_POINT ( 'NONE',  ( -68.65188857983726223, -23.48786465467241058, 11.44779295918254824 ) ) ;
#53936=CARTESIAN_POINT ( 'NONE',  ( -10.67548511050313209, -17.69376651829569269, -1.500000000000002220 ) ) ;
#53938=CARTESIAN_POINT ( 'NONE',  ( -11.89702471719568244, -18.04982639819725776, 11.49999999999999645 ) ) ;
#53939=VERTEX_POINT ( 'NONE', #14658 ) ;
#53941=DIRECTION ( 'NONE',  ( -3.773278334453079618E-23, 0.9999999999976377785, 2.173523156925979552E-06 ) ) ;
#53943=CARTESIAN_POINT ( 'NONE',  ( -11.68221627493902126, 19.09626523228051553, 11.49999999999998934 ) ) ;
#53945=CARTESIAN_POINT ( 'NONE',  ( -79.95270946814521551, -25.27875063563014635, 6.976216295041854920 ) ) ;
#53946=CARTESIAN_POINT ( 'NONE',  ( -53.52287095715008292, -23.94994826722564696, -0.6494450866342736939 ) ) ;
#53948=CARTESIAN_POINT ( 'NONE',  ( -99.53084541754070358, -25.27941189621985885, 4.062821213280528809 ) ) ;
#53949=CARTESIAN_POINT ( 'NONE',  ( -35.57119075587628032, -25.00182538069146787, 7.747789668545037145 ) ) ;
#53950=AXIS2_PLACEMENT_3D ( 'NONE', #72227, #4211, #35165 ) ;
#53951=DIRECTION ( 'NONE',  ( 3.773278334444166432E-23, -1.000000000000000000, 0.000000000000000000 ) ) ;
#53952=CARTESIAN_POINT ( 'NONE',  ( 16.15719879640481338, -13.26386290209467944, -1.500000000000002220 ) ) ;
#53954=CARTESIAN_POINT ( 'NONE',  ( -98.62287095715005592, -24.64898659630529210, 1.056161002820829697 ) ) ;
#53955=EDGE_LOOP ( 'NONE', ( #37195, #92932, #50441, #78682 ) ) ;
#53956=CARTESIAN_POINT ( 'NONE',  ( -109.5521097922329261, -24.35071581493543391, 9.817618358456025263 ) ) ;
#53957=CARTESIAN_POINT ( 'NONE',  ( -19.38594737788604405, 8.525550480899875438, -1.500000000000002220 ) ) ;
#53959=LINE ( 'NONE', #54956, #52701 ) ;
#53961=CARTESIAN_POINT ( 'NONE',  ( -3.523925741820590929, 21.50064390955241578, 11.49999999999998934 ) ) ;
#53962=DIRECTION ( 'NONE',  ( 0.000000000000000000, -2.173523156925980399E-06, 0.9999999999976378895 ) ) ;
#53963=CARTESIAN_POINT ( 'NONE',  ( -127.4728709571500360, -25.30558663486607429, 5.000950657679038791 ) ) ;
#53964=CARTESIAN_POINT ( 'NONE',  ( -80.22287095715005023, -23.47593901973090169, -1.443836447538997092 ) ) ;
#53965=CARTESIAN_POINT ( 'NONE',  ( 19.23208339725441007, -10.27600428404867827, -1.500000000000002220 ) ) ;
#53966=CARTESIAN_POINT ( 'NONE',  ( -71.22803624472236095, -25.31639477183338727, 4.920688597080680182 ) ) ;
#53968=CARTESIAN_POINT ( 'NONE',  ( -41.62287095715005592, -24.33832256527048088, 0.1851278514138586795 ) ) ;
#53969=CARTESIAN_POINT ( 'NONE',  ( -81.52287095715006160, -29.50250243563736774, 8.947779886222141599 ) ) ;
#53971=ORIENTED_EDGE ( 'NONE', *, *, #50774, .T. ) ;
#53977=CARTESIAN_POINT ( 'NONE',  ( -126.5228709571500616, -23.47596703998600631, 11.44779298504227683 ) ) ;
#53978=CARTESIAN_POINT ( 'NONE',  ( -17.78888362263414535, -11.56919986243916654, 11.49999999999998934 ) ) ;
#53979=CARTESIAN_POINT ( 'NONE',  ( -94.51280176992308668, -24.15543982623907482, -0.2315651400026595141 ) ) ;
#53980=CARTESIAN_POINT ( 'NONE',  ( -79.25918010276897974, -25.03138170620638192, 6.969965952212820781 ) ) ;
#53981=CARTESIAN_POINT ( 'NONE',  ( -99.62287095715005592, -24.64898659630367916, 1.056161002820829697 ) ) ;
#53984=CARTESIAN_POINT ( 'NONE',  ( -15.38109395195050233, 11.78095549196778258, -1.500000000000002220 ) ) ;
#53985=CARTESIAN_POINT ( 'NONE',  ( -39.03228499389064154, -25.11539320593059443, 2.804431443241629740 ) ) ;
#53986=ORIENTED_EDGE ( 'NONE', *, *, #50918, .T. ) ;
#53987=CARTESIAN_POINT ( 'NONE',  ( 16.42231304340664266, 10.40281881132301045, 11.49999999999999645 ) ) ;
#53988=DIRECTION ( 'NONE',  ( 3.773278334444166432E-23, -1.000000000000000000, 0.000000000000000000 ) ) ;
#53989=VECTOR ( 'NONE', #18764, 1000.000000000000114 ) ;
#53990=CARTESIAN_POINT ( 'NONE',  ( -56.62287095715005592, -29.50248528299804818, 1.056150453629034924 ) ) ;
#53993=DIRECTION ( 'NONE',  ( 1.000000000000000000, 3.773278334444167608E-23, 8.201307833595939069E-29 ) ) ;
#53994=CARTESIAN_POINT ( 'NONE',  ( -31.62287095715005236, -29.50248528299804818, 1.056150453629029817 ) ) ;
#53995=CARTESIAN_POINT ( 'NONE',  ( -101.1673844919198899, -25.22725712084274008, 3.624116959731904952 ) ) ;
#53996=CARTESIAN_POINT ( 'NONE',  ( -6.723608784814384620, 18.44229941887336821, -1.500000000000002220 ) ) ;
#53999=ORIENTED_EDGE ( 'NONE', *, *, #62372, .F. ) ;
#54000=CARTESIAN_POINT ( 'NONE',  ( 15.64208908530913256, 14.88810259432246852, 11.49999999999998934 ) ) ;
#54002=CARTESIAN_POINT ( 'NONE',  ( -130.5728709571500588, -23.56000036390797092, -1.497999999999531040 ) ) ;
#54004=CARTESIAN_POINT ( 'NONE',  ( 13.09964176094197441, 18.96253433080681106, -1.500000000000002220 ) ) ;
#54005=EDGE_CURVE ( 'NONE', #51171, #61052, #86090, .T. ) ;
#54007=DIRECTION ( 'NONE',  ( -3.773278334453079618E-23, 0.9999999999976377785, 2.173523156925979975E-06 ) ) ;
#54009=LINE ( 'NONE', #31650, #31667 ) ;
#54010=CARTESIAN_POINT ( 'NONE',  ( -64.62287095715005592, -23.48786465467241413, 11.44779295918254824 ) ) ;
#54013=CARTESIAN_POINT ( 'NONE',  ( -114.6244179104245688, -24.51419770103159124, 9.386484678747160970 ) ) ;
#54014=CARTESIAN_POINT ( 'NONE',  ( 7.614665684681447111, -18.39110272641453037, -1.500000000000002220 ) ) ;
#54017=ADVANCED_FACE ( 'NONE', ( #20761 ), #76051, .T. ) ;
#54018=CARTESIAN_POINT ( 'NONE',  ( 9.171884637996585710, -17.55225146786146695, -1.500000000000002220 ) ) ;
#54019=EDGE_CURVE ( 'NONE', #50012, #60701, #33977, .T. ) ;
#54020=CARTESIAN_POINT ( 'NONE',  ( -56.60507748122925165, -23.73766607897670511, -1.055555164236459342 ) ) ;
#54021=EDGE_CURVE ( 'NONE', #24252, #503, #27891, .T. ) ;
#54023=UNCERTAINTY_MEASURE_WITH_UNIT (LENGTH_MEASURE( 1.000000000000000082E-05 ), #16563, 'distance_accuracy_value', 'NONE');
#54026=DIRECTION ( 'NONE',  ( -3.773278334453079618E-23, 0.9999999999976377785, 2.173523156925979975E-06 ) ) ;
#54027=CARTESIAN_POINT ( 'NONE',  ( -5.954758479537505700, 19.85987847461844424, 11.49999999999999645 ) ) ;
#54029=CARTESIAN_POINT ( 'NONE',  ( -49.68170153635294639, -25.31439325082426706, 5.417898099858684091 ) ) ;
#54030=CARTESIAN_POINT ( 'NONE',  ( 15.01325480956343483, 17.08929600257393489, 11.49999999999999645 ) ) ;
#54032=PLANE ( 'NONE',  #38149 ) ;
#54033=CARTESIAN_POINT ( 'NONE',  ( -52.62287095715004170, -23.47596703998600276, 11.44779298504227505 ) ) ;
#54034=CARTESIAN_POINT ( 'NONE',  ( 20.15506735835773000, -1.303320585059813741, -1.500000000000002220 ) ) ;
#54035=ADVANCED_FACE ( 'NONE', ( #82176 ), #52329, .T. ) ;
#54036=CARTESIAN_POINT ( 'NONE',  ( -29.81175120719462512, -25.25636103033882307, 4.942810967025194735 ) ) ;
#54037=CARTESIAN_POINT ( 'NONE',  ( -95.62287095715007013, -24.14321612903115621, -0.2833117244521696776 ) ) ;
#54038=ORIENTED_EDGE ( 'NONE', *, *, #63686, .F. ) ;
#54042=CARTESIAN_POINT ( 'NONE',  ( -33.52287095715006160, -24.64965694238574656, 8.947790433994207149 ) ) ;
#54043=CARTESIAN_POINT ( 'NONE',  ( 22.59171682324826236, -3.780823453261925593, -1.500000000000002220 ) ) ;
#54044=CARTESIAN_POINT ( 'NONE',  ( -51.04387771620785941, -25.18439694560420250, 3.499820392625150767 ) ) ;
#54045=CARTESIAN_POINT ( 'NONE',  ( 10.55456386191721663, 18.89434267519128596, -1.500000000000002220 ) ) ;
#54048=CARTESIAN_POINT ( 'NONE',  ( -8.544475976622297964, 19.10969517993760292, 11.49999999999999645 ) ) ;
#54050=CARTESIAN_POINT ( 'NONE',  ( -69.15592802969443653, -25.24754373336818603, 5.438241903594629001 ) ) ;
#54051=CARTESIAN_POINT ( 'NONE',  ( -17.76638496452178018, -13.01238552544781335, -1.500000000000002220 ) ) ;
#54053=DIRECTION ( 'NONE',  ( -3.773278334453079618E-23, 0.9999999999976377785, 2.173523156925979975E-06 ) ) ;
#54054=CARTESIAN_POINT ( 'NONE',  ( -30.47287095715008576, -23.47593902499770380, -1.441415665115638456 ) ) ;
#54058=CARTESIAN_POINT ( 'NONE',  ( -122.6228709571501128, -23.95044443724993144, 10.65354141964649948 ) ) ;
#54060=CARTESIAN_POINT ( 'NONE',  ( -72.54966452413839306, -24.15620529776627734, 10.23563542870660825 ) ) ;
#54061=ORIENTED_EDGE ( 'NONE', *, *, #80626, .F. ) ;
#54062=AXIS2_PLACEMENT_3D ( 'NONE', #62589, #56988, #58485 ) ;
#54064=CARTESIAN_POINT ( 'NONE',  ( -71.50227123732281598, -24.35071581493543391, 9.817618358456021710 ) ) ;
#54067=CARTESIAN_POINT ( 'NONE',  ( 17.75789855128238770, 10.12834119215567164, -1.500000000000002220 ) ) ;
#54068=EDGE_CURVE ( 'NONE', #85746, #15522, #61848, .T. ) ;
#54069=VERTEX_POINT ( 'NONE', #30384 ) ;
#54070=CARTESIAN_POINT ( 'NONE',  ( -99.29687923781919778, -25.25133594952260552, 6.149712203147405631 ) ) ;
#54073=CARTESIAN_POINT ( 'NONE',  ( 15.07672925556244969, 16.42598562245719407, 11.49999999999998934 ) ) ;
#54076=CARTESIAN_POINT ( 'NONE',  ( -88.62287095715011276, -24.51387760970723662, 9.387446482453407626 ) ) ;
#54077=ORIENTED_EDGE ( 'NONE', *, *, #83125, .T. ) ;
#54080=CARTESIAN_POINT ( 'NONE',  ( -39.52287095715006160, -24.35013146730202749, 9.818937971375113705 ) ) ;
#54081=CARTESIAN_POINT ( 'NONE',  ( -18.54028579900546703, -9.471972883075929772, 11.49999999999998934 ) ) ;
#54084=ORIENTED_EDGE ( 'NONE', *, *, #49391, .F. ) ;
#54085=B_SPLINE_SURFACE_WITH_KNOTS ( 'NONE', 3, 3, ( 
 ( #85167, #86670, #15655, #85673 ),
 ( #16153, #47124, #55244, #78037 ),
 ( #8550, #78543, #39504, #939 ),
 ( #86170, #39998, #32386, #24761 ),
 ( #17158, #48124, #79053, #9546 ),
 ( #40509, #51113, #35882, #80059 ),
 ( #19648, #97283, #10544, #49628 ) ),
 .UNSPECIFIED., .F., .F., .F.,
 ( 4, 3, 4 ),
 ( 4, 4 ),
 ( 0.0004766839783834679817, 0.1029713700210900945, 0.2054660560637967259 ),
 ( 0.9297305048046913267, 0.9311722053073241412 ),
 .UNSPECIFIED. ) ;
#54086=CARTESIAN_POINT ( 'NONE',  ( -98.52287095715010423, -23.96177878511310055, 10.65340807706329507 ) ) ;
#54088=ORIENTED_EDGE ( 'NONE', *, *, #17753, .T. ) ;
#54090=CARTESIAN_POINT ( 'NONE',  ( -121.6228709571500417, -23.48786465467241769, 11.44779295918253759 ) ) ;
#54092=CARTESIAN_POINT ( 'NONE',  ( -40.62287095715004881, -24.63345952396255356, 9.038047939301508293 ) ) ;
#54093=CARTESIAN_POINT ( 'NONE',  ( -92.58398631988276861, -24.66019654487200441, 8.947790411086112172 ) ) ;
#54095=CARTESIAN_POINT ( 'NONE',  ( 8.998109643811913472, -20.30750954041392120, 11.49999999999999645 ) ) ;
#54096=EDGE_LOOP ( 'NONE', ( #56386, #81388, #60727, #44989 ) ) ;
#54098=ORIENTED_EDGE ( 'NONE', *, *, #73745, .F. ) ;
#54100=CARTESIAN_POINT ( 'NONE',  ( 22.15051849217804403, -4.756829024181505439, -1.500000000000002220 ) ) ;
#54101=CARTESIAN_POINT ( 'NONE',  ( -115.5222181624795041, -23.48786465467241769, 11.44779295918253581 ) ) ;
#54103=B_SPLINE_CURVE_WITH_KNOTS ( 'NONE', 3,
 ( #19838, #36081, #28456, #34591, #26967, #50318 ),
 .UNSPECIFIED., .F., .F.,
 ( 4, 2, 4 ),
 ( 1.570887131794333942E-05, 0.001396322306279758904, 0.002776935741241574537 ),
 .UNSPECIFIED. ) ;
#54107=B_SPLINE_CURVE_WITH_KNOTS ( 'NONE', 3,
 ( #63411, #24814, #46167, #94329 ),
 .UNSPECIFIED., .F., .F.,
 ( 4, 4 ),
 ( 0.008760056121740519147, 0.009760803162505871794 ),
 .UNSPECIFIED. ) ;
#54108=CARTESIAN_POINT ( 'NONE',  ( -12.53166870608491479, 15.75175023352509385, -1.500000000000002220 ) ) ;
#54109=CARTESIAN_POINT ( 'NONE',  ( -121.6228709571500417, -29.50247984919015209, -1.443849546365046699 ) ) ;
#54110=ORIENTED_EDGE ( 'NONE', *, *, #37404, .T. ) ;
#54111=DIRECTION ( 'NONE',  ( -1.000000000000000000, -3.773278334444167608E-23, -8.201307833595939069E-29 ) ) ;
#54112=CARTESIAN_POINT ( 'NONE',  ( 21.65046080595755740, -5.567969076317650590, -1.500000000000002220 ) ) ;
#54114=ORIENTED_EDGE ( 'NONE', *, *, #89045, .F. ) ;
#54116=DIRECTION ( 'NONE',  ( -3.773278334453079618E-23, 0.9999999999976377785, 2.173523156925979552E-06 ) ) ;
#54117=CARTESIAN_POINT ( 'NONE',  ( -94.50572660452756679, -24.66019654487199730, 8.947790411086121054 ) ) ;
#54119=CARTESIAN_POINT ( 'NONE',  ( -116.5228709571500474, -24.50321055353805377, 9.387540953477515160 ) ) ;
#54120=FACE_BOUND ( 'NONE', #12833, .T. ) ;
#54121=CARTESIAN_POINT ( 'NONE',  ( 15.80261042061247068, 11.49252619723154112, 11.49999999999998934 ) ) ;
#54123=CARTESIAN_POINT ( 'NONE',  ( -0.9917595143200197416, 21.46465604038169772, -1.500000000000002220 ) ) ;
#54124=CARTESIAN_POINT ( 'NONE',  ( -36.55620429048339304, -23.47593901973091235, -1.443836447539011525 ) ) ;
#54128=CARTESIAN_POINT ( 'NONE',  ( 11.15996004898972771, 19.99216496293481882, -1.500000000000002220 ) ) ;
#54130=FACE_OUTER_BOUND ( 'NONE', #78726, .T. ) ;
#54132=CARTESIAN_POINT ( 'NONE',  ( -19.63739455291241498, 3.909132673056371132, 11.49999999999999645 ) ) ;
#54133=CARTESIAN_POINT ( 'NONE',  ( -79.16633218095056179, -25.31594453621216090, 5.138964353779805094 ) ) ;
#54134=DIRECTION ( 'NONE',  ( 1.000000000000000000, 3.773278334444166432E-23, 8.201307841325785021E-29 ) ) ;
#54135=ADVANCED_FACE ( 'NONE', ( #70961 ), #46627, .T. ) ;
#54139=VERTEX_POINT ( 'NONE', #62867 ) ;
#54140=B_SPLINE_CURVE_WITH_KNOTS ( 'NONE', 3,
 ( #40768, #95558, #92178, #71729 ),
 .UNSPECIFIED., .F., .F.,
 ( 4, 4 ),
 ( 0.000000000000000000, 0.0001000000000000028644 ),
 .UNSPECIFIED. ) ;
#54141=CARTESIAN_POINT ( 'NONE',  ( -120.5228709571500616, -29.50250243563736774, 8.947779886222134493 ) ) ;
#54142=DIRECTION ( 'NONE',  ( -3.773278334453079618E-23, 0.9999999999976377785, 2.173523156925979975E-06 ) ) ;
#54144=CARTESIAN_POINT ( 'NONE',  ( -18.02536786162489335, -12.12045427182966861, 11.49999999999998934 ) ) ;
#54145=CARTESIAN_POINT ( 'NONE',  ( -88.62287095715004170, -23.47596703998600631, 11.44779298504227860 ) ) ;
#54146=CARTESIAN_POINT ( 'NONE',  ( -19.61951575358169819, -0.1233725505697131491, -1.500000000000002220 ) ) ;
#54147=EDGE_CURVE ( 'NONE', #96665, #29762, #3808, .T. ) ;
#54148=CARTESIAN_POINT ( 'NONE',  ( -85.52287095715006160, -23.48786465467241058, 11.44779295918254292 ) ) ;
#54150=CARTESIAN_POINT ( 'NONE',  ( -109.4462232385598099, -25.31698038172532605, 4.635298210512930339 ) ) ;
#54152=CARTESIAN_POINT ( 'NONE',  ( -91.55809090141561057, -23.73791477778912196, 11.05961554403170410 ) ) ;
#54154=CARTESIAN_POINT ( 'NONE',  ( 18.67943556539783856, 8.552475402716291697, 11.49999999999999645 ) ) ;
#54155=CARTESIAN_POINT ( 'NONE',  ( -39.15087641650215744, -25.31438038583802808, 4.798588888368600536 ) ) ;
#54157=ORIENTED_EDGE ( 'NONE', *, *, #88043, .T. ) ;
#54158=CARTESIAN_POINT ( 'NONE',  ( -83.62287095715007013, -23.47596703998600631, 11.44779298504227860 ) ) ;
#54162=EDGE_CURVE ( 'NONE', #22234, #64167, #50614, .T. ) ;
#54163=CARTESIAN_POINT ( 'NONE',  ( -25.81215951358583993, -24.61459805061084793, 6.831252646531839723 ) ) ;
#54164=AXIS2_PLACEMENT_3D ( 'NONE', #16713, #47681, #79110 ) ;
#54166=B_SPLINE_CURVE_WITH_KNOTS ( 'NONE', 3,
 ( #73612, #71617, #87839, #25932 ),
 .UNSPECIFIED., .F., .F.,
 ( 4, 4 ),
 ( 0.000000000000000000, 0.0001000000000000028644 ),
 .UNSPECIFIED. ) ;
#54168=CARTESIAN_POINT ( 'NONE',  ( -22.63574357292403860, -4.499050354539342322, 11.49999999999999645 ) ) ;
#54169=CARTESIAN_POINT ( 'NONE',  ( -18.69919181139871966, -13.08804974640095686, -1.500000000000002220 ) ) ;
#54172=DIRECTION ( 'NONE',  ( -3.773278334453079618E-23, 0.9999999999976377785, 2.173523156925979975E-06 ) ) ;
#54173=CARTESIAN_POINT ( 'NONE',  ( -64.52287095715006160, -23.47593901973090169, -1.443836447538996870 ) ) ;
#54174=CARTESIAN_POINT ( 'NONE',  ( 11.36419782745769069, 19.35538867594532775, 11.49999999999999645 ) ) ;
#54176=DIRECTION ( 'NONE',  ( -3.773278334453080206E-23, 0.9999999999976377785, 2.173523156925979975E-06 ) ) ;
#54177=CARTESIAN_POINT ( 'NONE',  ( -43.60020673645048817, -23.96119346886880663, -0.6495511937831988103 ) ) ;
#54178=CARTESIAN_POINT ( 'NONE',  ( -16.24880213243413607, 14.73142910551002238, 11.49999999999998934 ) ) ;
#54180=CARTESIAN_POINT ( 'NONE',  ( -87.50495267027400814, -24.51419770103156281, 9.386484678747175181 ) ) ;
#54181=CARTESIAN_POINT ( 'NONE',  ( -104.5103228290961681, -24.65952944569304606, 1.056160979905702346 ) ) ;
#54183=DIRECTION ( 'NONE',  ( -3.773278334453080206E-23, 0.9999999999976377785, 2.173523156925979975E-06 ) ) ;
#54185=CARTESIAN_POINT ( 'NONE',  ( -15.50425215161893355, 13.37805140191733777, 11.49999999999998934 ) ) ;
#54186=EDGE_LOOP ( 'NONE', ( #84032, #94747, #39206, #93733 ) ) ;
#54187=ORIENTED_EDGE ( 'NONE', *, *, #15907, .T. ) ;
#54189=EDGE_LOOP ( 'NONE', ( #95587, #67924, #54088, #71203 ) ) ;
#54190=CARTESIAN_POINT ( 'NONE',  ( -22.67921066581790868, 4.291001918001082771, -1.500000000000002220 ) ) ;
#54191=DIRECTION ( 'NONE',  ( 0.000000000000000000, 0.9999999999976377785, 2.173523156925979128E-06 ) ) ;
#54192=CARTESIAN_POINT ( 'NONE',  ( -6.898722100468609675, -19.10483383855023476, -1.500000000000002220 ) ) ;
#54194=CARTESIAN_POINT ( 'NONE',  ( -30.64751926837171325, -23.47596703998600631, 11.44779298504228038 ) ) ;
#54195=CARTESIAN_POINT ( 'NONE',  ( -92.63717942627289403, -23.73766607897671221, -1.055555164236430477 ) ) ;
#54196=EDGE_CURVE ( 'NONE', #38068, #46271, #36493, .T. ) ;
#54197=CARTESIAN_POINT ( 'NONE',  ( -101.3873120667114733, -25.20683408230442879, 6.626510787099375577 ) ) ;
#54198=CARTESIAN_POINT ( 'NONE',  ( -70.52205928114219091, -23.48783264082477018, -1.443836473390095021 ) ) ;
#54199=CARTESIAN_POINT ( 'NONE',  ( -14.25192491085926072, -16.12266454619898326, 11.49999999999999645 ) ) ;
#54200=ORIENTED_EDGE ( 'NONE', *, *, #90669, .T. ) ;
#54201=CARTESIAN_POINT ( 'NONE',  ( -75.50251933352205924, -24.40034930558991277, 0.3402023900116102895 ) ) ;
#54203=ORIENTED_EDGE ( 'NONE', *, *, #70286, .T. ) ;
#54204=CARTESIAN_POINT ( 'NONE',  ( 17.59156710592704442, 10.99281682905060897, 11.49999999999998934 ) ) ;
#54205=ADVANCED_FACE ( 'NONE', ( #71464 ), #87679, .F. ) ;
#54208=ORIENTED_EDGE ( 'NONE', *, *, #70046, .T. ) ;
#54209=FACE_OUTER_BOUND ( 'NONE', #84458, .T. ) ;
#54210=CARTESIAN_POINT ( 'NONE',  ( -53.52287095715006870, -23.96127896941631263, -0.6493128931038055773 ) ) ;
#54211=ORIENTED_EDGE ( 'NONE', *, *, #26294, .T. ) ;
#54214=PLANE ( 'NONE',  #17335 ) ;
#54215=CARTESIAN_POINT ( 'NONE',  ( -124.5228709571500616, -23.48786465467241769, 11.44779295918253759 ) ) ;
#54216=CARTESIAN_POINT ( 'NONE',  ( 18.54397492014093984, 11.73900455106235086, 11.49999999999999645 ) ) ;
#54218=CARTESIAN_POINT ( 'NONE',  ( 4.940617368476682536, -22.01678987175928981, 11.49999999999998934 ) ) ;
#54219=CARTESIAN_POINT ( 'NONE',  ( -5.413507703253908510, 20.27406835261982465, -1.500000000000002220 ) ) ;
#54224=FACE_OUTER_BOUND ( 'NONE', #42994, .T. ) ;
#54226=CARTESIAN_POINT ( 'NONE',  ( -15.45034113870702441, -14.97902827799142500, -1.500000000000002220 ) ) ;
#54227=CARTESIAN_POINT ( 'NONE',  ( -57.52287095715005449, -24.64898659630528854, 1.056161002820822592 ) ) ;
#54229=CARTESIAN_POINT ( 'NONE',  ( 3.428800225705347149, -20.88102749682517612, 11.49999999999998934 ) ) ;
#54231=CARTESIAN_POINT ( 'NONE',  ( -61.66815417520224685, -25.03722704563418944, 7.590184509431679771 ) ) ;
#54232=CARTESIAN_POINT ( 'NONE',  ( -64.62287095715005592, -23.47593901973091235, -1.443836447539007972 ) ) ;
#54233=CARTESIAN_POINT ( 'NONE',  ( -52.22287095715005023, -23.47593901973090169, -1.443836447538997758 ) ) ;
#54234=CARTESIAN_POINT ( 'NONE',  ( -101.5228709571500758, -24.65952944569304606, 1.056160979905702346 ) ) ;
#54235=CARTESIAN_POINT ( 'NONE',  ( 13.35222405703702186, 17.66689192352044913, -1.500000000000002220 ) ) ;
#54236=CARTESIAN_POINT ( 'NONE',  ( -71.56490542036905822, -23.48783264082477018, -1.443836473390092578 ) ) ;
#54240=FACE_OUTER_BOUND ( 'NONE', #23465, .T. ) ;
#54241=CARTESIAN_POINT ( 'NONE',  ( -126.5905539433028792, -23.73766607897670156, -1.055555164236450016 ) ) ;
#54242=CARTESIAN_POINT ( 'NONE',  ( -76.52287095715007581, -23.47593901973090169, -1.443836447538996648 ) ) ;
#54244=CARTESIAN_POINT ( 'NONE',  ( 17.65527434030279252, -8.155491144718855168, -1.500000000000002220 ) ) ;
#54245=CARTESIAN_POINT ( 'NONE',  ( -21.04715019690976874, -3.721878931196799467, 11.49999999999998934 ) ) ;
#54247=B_SPLINE_CURVE_WITH_KNOTS ( 'NONE', 3,
 ( #27090, #34211, #26086, #63676, #94596, #25077, #48938, #2766 ),
 .UNSPECIFIED., .F., .F.,
 ( 4, 2, 2, 4 ),
 ( -0.001240666984355838021, -0.0002401179793394964124, 0.0007604310256768451962, 0.002761529035709528630 ),
 .UNSPECIFIED. ) ;
#54250=CARTESIAN_POINT ( 'NONE',  ( -44.52287095715006870, -24.33927499327855060, 9.819080762295804732 ) ) ;
#54251=CARTESIAN_POINT ( 'NONE',  ( 2.290073164716609710, 22.57640404599860418, -1.500000000000002220 ) ) ;
#54252=CARTESIAN_POINT ( 'NONE',  ( -124.5228709571500616, -23.48786465467241769, 11.44779295918253759 ) ) ;
#54253=CARTESIAN_POINT ( 'NONE',  ( -127.6228709571500559, -24.51283580621365843, 0.6167428607019918019 ) ) ;
#54254=CARTESIAN_POINT ( 'NONE',  ( -0.2410636032128395945, 19.88167143085883737, 11.49999999999999645 ) ) ;
#54255=ADVANCED_FACE ( 'NONE', ( #27281 ), #99316, .T. ) ;
#54257=ORIENTED_EDGE ( 'NONE', *, *, #31541, .T. ) ;
#54258=DIRECTION ( 'NONE',  ( 0.000000000000000000, 0.9999999999976377785, 2.173523156925979975E-06 ) ) ;
#54259=LINE ( 'NONE', #70476, #11801 ) ;
#54260=EDGE_CURVE ( 'NONE', #46797, #87999, #21909, .T. ) ;
#54261=CARTESIAN_POINT ( 'NONE',  ( -68.52287095715004739, -23.73907113216989373, -1.053371485793255014 ) ) ;
#54262=CARTESIAN_POINT ( 'NONE',  ( 10.55456386191721663, 18.89434267519128596, 11.49999999999998934 ) ) ;
#54263=CARTESIAN_POINT ( 'NONE',  ( -56.57854487595048454, -24.66019654487199375, 8.947790411086122830 ) ) ;
#54264=CARTESIAN_POINT ( 'NONE',  ( -9.780116039169133302, 16.78644576961053048, -1.500000000000002220 ) ) ;
#54268=CARTESIAN_POINT ( 'NONE',  ( 8.478510716907816658, 17.93336729499101523, -1.500000000000002220 ) ) ;
#54269=EDGE_LOOP ( 'NONE', ( #9777, #64795, #61959, #49363 ) ) ;
#54270=EDGE_CURVE ( 'NONE', #33481, #82250, #67345, .T. ) ;
#54272=CARTESIAN_POINT ( 'NONE',  ( 13.49383759531269433, -15.17088004136028090, 11.49999999999999645 ) ) ;
#54273=DIRECTION ( 'NONE',  ( -3.773278334444167608E-23, 1.000000000000000000, 0.000000000000000000 ) ) ;
#54274=EDGE_CURVE ( 'NONE', #19368, #71172, #89692, .T. ) ;
#54275=PLANE ( 'NONE',  #57782 ) ;
#54277=B_SPLINE_SURFACE_WITH_KNOTS ( 'NONE', 3, 3, ( 
 ( #23927, #47280, #9202, #34927 ),
 ( #70609, #65904, #71119, #55906 ),
 ( #40671, #1609, #32547, #1102 ),
 ( #63519, #96820, #94442, #24928 ),
 ( #86829, #79214, #9714, #33056 ),
 ( #64034, #94948, #97812, #37426 ),
 ( #20186, #99310, #28307, #75964 ) ),
 .UNSPECIFIED., .F., .F., .F.,
 ( 4, 3, 4 ),
 ( 4, 4 ),
 ( 0.7945040050992238090, 0.8970133687736496775, 0.9995227324480754350 ),
 ( 0.1395294536136304497, 0.1406065942234439314 ),
 .UNSPECIFIED. ) ;
#54278=CARTESIAN_POINT ( 'NONE',  ( -30.61275986115374437, -24.37728322581795481, 9.960208392924579712 ) ) ;
#54279=PLANE ( 'NONE',  #55819 ) ;
#54280=CARTESIAN_POINT ( 'NONE',  ( -49.13746579462012676, -25.25214525603300331, 5.391919962994458970 ) ) ;
#54281=CARTESIAN_POINT ( 'NONE',  ( -40.67673042091735880, -23.48786465467240347, 11.44779295918255180 ) ) ;
#54283=CARTESIAN_POINT ( 'NONE',  ( 8.649182803842551337, -18.14983140373652404, -1.500000000000002220 ) ) ;
#54284=CARTESIAN_POINT ( 'NONE',  ( -129.5228709571499905, -23.48783264082477729, -1.443836473390079700 ) ) ;
#54285=ORIENTED_EDGE ( 'NONE', *, *, #48887, .T. ) ;
#54286=B_SPLINE_CURVE_WITH_KNOTS ( 'NONE', 3,
 ( #77848, #68395, #45564, #22193, #86477, #75984 ),
 .UNSPECIFIED., .F., .F.,
 ( 4, 2, 4 ),
 ( 1.570887131794795405E-05, 0.001396322306279761940, 0.002776935741241575838 ),
 .UNSPECIFIED. ) ;
#54287=CARTESIAN_POINT ( 'NONE',  ( -36.52287095715009002, -24.33832256527048088, 0.1851278514138557096 ) ) ;
#54288=ADVANCED_FACE ( 'NONE', ( #82550 ), #4936, .T. ) ;
#54289=CARTESIAN_POINT ( 'NONE',  ( -12.24191887126339751, 19.33842681661653984, 11.49999999999999645 ) ) ;
#54290=CARTESIAN_POINT ( 'NONE',  ( -9.076218414377828836, -20.82814578352222767, -1.500000000000002220 ) ) ;
#54292=CARTESIAN_POINT ( 'NONE',  ( -45.52287095715006160, -24.92579138211019085, 1.929029949965659130 ) ) ;
#54293=DIRECTION ( 'NONE',  ( 1.000000000000000000, 3.773278334444167020E-23, 8.201307838832447938E-29 ) ) ;
#54294=CARTESIAN_POINT ( 'NONE',  ( -64.62287095715005592, -29.50250786944525672, 11.44777988621623876 ) ) ;
#54297=CARTESIAN_POINT ( 'NONE',  ( -128.5895400625830405, -24.51419770103157703, 9.386484678747171628 ) ) ;
#54300=CARTESIAN_POINT ( 'NONE',  ( 19.51578053514377586, 5.923290232019536639, 11.49999999999998934 ) ) ;
#54301=VERTEX_POINT ( 'NONE', #74445 ) ;
#54302=CARTESIAN_POINT ( 'NONE',  ( -22.87025945403008365, 2.249016246415321163, -1.500000000000002220 ) ) ;
#54303=CARTESIAN_POINT ( 'NONE',  ( -54.55345688732126774, -23.96169478059712787, 10.65365249895718947 ) ) ;
#54308=CARTESIAN_POINT ( 'NONE',  ( -81.41734784726033070, -25.22106677559741783, 6.517144941221712173 ) ) ;
#54309=CARTESIAN_POINT ( 'NONE',  ( -51.50747100937991263, -23.96169478059712787, 10.65365249895718236 ) ) ;
#54310=CARTESIAN_POINT ( 'NONE',  ( 12.11089201280794470, -17.53110042540249225, 11.49999999999999645 ) ) ;
#54311=ORIENTED_EDGE ( 'NONE', *, *, #32480, .F. ) ;
#54313=CARTESIAN_POINT ( 'NONE',  ( -4.330935931041660858, -21.79039167146679290, -1.500000000000002220 ) ) ;
#54314=CARTESIAN_POINT ( 'NONE',  ( 19.88596897151998633, -5.565664080715476913, -1.500000000000002220 ) ) ;
#54317=CARTESIAN_POINT ( 'NONE',  ( -109.6203743360497214, -25.27682868748497569, 5.518883987748085751 ) ) ;
#54319=CARTESIAN_POINT ( 'NONE',  ( -95.52214753415771042, -23.48786465467241058, 11.44779295918254469 ) ) ;
#54321=CARTESIAN_POINT ( 'NONE',  ( -49.31664351742390551, -25.23350000577289620, 6.415014328141102062 ) ) ;
#54323=CARTESIAN_POINT ( 'NONE',  ( -76.62287095715007013, -29.50250243563736774, 8.947779886222141599 ) ) ;
#54324=CARTESIAN_POINT ( 'NONE',  ( -116.5228709571500616, -23.47596703998600631, 11.44779298504227860 ) ) ;
#54325=CARTESIAN_POINT ( 'NONE',  ( -6.767879454864726974, -19.68250801024624508, -1.500000000000002220 ) ) ;
#54326=CARTESIAN_POINT ( 'NONE',  ( 20.45693200876408469, 7.529271608661172621, 11.49999999999999645 ) ) ;
#54327=ADVANCED_FACE ( 'NONE', ( #15402 ), #46362, .T. ) ;
#54328=PLANE ( 'NONE',  #43139 ) ;
#54329=CARTESIAN_POINT ( 'NONE',  ( -78.63378921853097836, -24.15620529776628445, 10.23563542870660292 ) ) ;
#54330=CARTESIAN_POINT ( 'NONE',  ( -21.13723655771239152, -7.639886366525781014, -1.500000000000002220 ) ) ;
#54331=CARTESIAN_POINT ( 'NONE',  ( -38.65668546529683880, -23.73766607897670511, -1.055555164236442689 ) ) ;
#54337=B_SPLINE_CURVE_WITH_KNOTS ( 'NONE', 3,
 ( #2123, #57416, #56914, #66036, #26454, #40676 ),
 .UNSPECIFIED., .F., .F.,
 ( 4, 2, 4 ),
 ( 0.000000000000000000, 0.001380901958385388545, 0.002761803916770777089 ),
 .UNSPECIFIED. ) ;
#54339=EDGE_LOOP ( 'NONE', ( #58395, #25846, #55809, #23395 ) ) ;
#54340=CARTESIAN_POINT ( 'NONE',  ( -1.376967878889499897, 21.29249089469206524, -1.500000000000002220 ) ) ;
#54341=VERTEX_POINT ( 'NONE', #43010 ) ;
#54342=CARTESIAN_POINT ( 'NONE',  ( -13.78326148797977169, 15.88460234914768421, 11.49999999999998934 ) ) ;
#54343=CARTESIAN_POINT ( 'NONE',  ( -30.60821039366259200, -24.48911842944947992, 0.5642940035406466270 ) ) ;
#54344=CARTESIAN_POINT ( 'NONE',  ( -111.0291780393114323, -25.22779283739988188, 3.542651572262693005 ) ) ;
#54346=CARTESIAN_POINT ( 'NONE',  ( -1.948345350117603125, -21.87844622001750139, -1.500000000000002220 ) ) ;
#54347=CARTESIAN_POINT ( 'NONE',  ( -0.1490770655183830395, -21.12008023607310037, -1.443836447538997536 ) ) ;
#54348=ORIENTED_EDGE ( 'NONE', *, *, #97795, .F. ) ;
#54349=PLANE ( 'NONE',  #54906 ) ;
#54350=CARTESIAN_POINT ( 'NONE',  ( -121.5228709571500616, -24.64898659630529565, 1.056161002820833028 ) ) ;
#54351=CARTESIAN_POINT ( 'NONE',  ( 0.5783248939474509021, 20.82821387695577187, 11.49999999999999645 ) ) ;
#54353=FACE_OUTER_BOUND ( 'NONE', #84356, .T. ) ;
#54354=CARTESIAN_POINT ( 'NONE',  ( -0.1051205485391842609, -21.68913189117569473, 10.47594215909544779 ) ) ;
#54355=CARTESIAN_POINT ( 'NONE',  ( 17.02398533174402218, 12.79255474601471043, 11.49999999999998934 ) ) ;
#54357=CARTESIAN_POINT ( 'NONE',  ( -107.5875550465913904, -24.51419770103157703, 9.386484678747169852 ) ) ;
#54361=CARTESIAN_POINT ( 'NONE',  ( -22.50818191331092777, 0.9639279967183422837, -1.500000000000002220 ) ) ;
#54366=CARTESIAN_POINT ( 'NONE',  ( -11.77723790057865116, -15.68276428244051779, 11.49999999999999645 ) ) ;
#54370=VECTOR ( 'NONE', #65216, 1000.000000000000114 ) ;
#54371=CARTESIAN_POINT ( 'NONE',  ( -99.59916881451887605, -23.48783264082478439, -1.443836473390062825 ) ) ;
#54372=DIRECTION ( 'NONE',  ( 3.773278334444166432E-23, -1.000000000000000000, 0.000000000000000000 ) ) ;
#54373=FACE_BOUND ( 'NONE', #50362, .T. ) ;
#54375=CARTESIAN_POINT ( 'NONE',  ( 9.261118129494249729, -17.44851725036260248, 11.49999999999998934 ) ) ;
#54377=EDGE_CURVE ( 'NONE', #20176, #43203, #17076, .T. ) ;
#54381=EDGE_LOOP ( 'NONE', ( #95353, #72444, #67566, #46429 ) ) ;
#54384=CARTESIAN_POINT ( 'NONE',  ( -55.58286566446923871, -24.73486907724917572, 1.287355809206962798 ) ) ;
#54386=CARTESIAN_POINT ( 'NONE',  ( -85.55620429048339304, -23.48783264082478084, -1.443836473390063269 ) ) ;
#54387=CARTESIAN_POINT ( 'NONE',  ( -44.58953762381673158, -24.64965694238406613, 8.947790433994660120 ) ) ;
#54388=CARTESIAN_POINT ( 'NONE',  ( -29.96442075442584851, -23.42317284524191123, -1.443836447538997314 ) ) ;
#54389=CARTESIAN_POINT ( 'NONE',  ( 19.86090765050778728, -2.328952942160339212, 11.49999999999998934 ) ) ;
#54391=FACE_OUTER_BOUND ( 'NONE', #53773, .T. ) ;
#54392=CARTESIAN_POINT ( 'NONE',  ( -45.63589775446569519, -24.63419186844611986, 9.035850630976927533 ) ) ;
#54396=PLANE ( 'NONE',  #7078 ) ;
#54397=CARTESIAN_POINT ( 'NONE',  ( -35.50852639300465086, -23.85016227208580730, -0.8807180028928170978 ) ) ;
#54398=CARTESIAN_POINT ( 'NONE',  ( -100.5228709571500758, -24.52323809116981934, 9.355190652339423707 ) ) ;
#54399=CARTESIAN_POINT ( 'NONE',  ( -118.8949105597723843, -25.34741607406076724, 3.801658267186116547 ) ) ;
#54400=DIRECTION ( 'NONE',  ( -0.000000000000000000, 2.173523156925979552E-06, -0.9999999999976378895 ) ) ;
#54401=DIRECTION ( 'NONE',  ( -1.000000000000000000, -3.773278334444166432E-23, -8.201307841325785021E-29 ) ) ;
#54403=ORIENTED_EDGE ( 'NONE', *, *, #25593, .T. ) ;
#54404=CARTESIAN_POINT ( 'NONE',  ( 20.05935882324986963, -3.104462954613115500, -1.500000000000002220 ) ) ;
#54406=CARTESIAN_POINT ( 'NONE',  ( -82.52287095715006160, -29.50250243563736774, 8.947779886222141599 ) ) ;
#54407=EDGE_LOOP ( 'NONE', ( #67150, #66062, #47705, #25058 ) ) ;
#54408=CARTESIAN_POINT ( 'NONE',  ( -81.62287095715005592, -24.65952944569304606, 1.056160979905699460 ) ) ;
#54410=CARTESIAN_POINT ( 'NONE',  ( 13.72940079880349984, -14.68433028913016791, -1.500000000000002220 ) ) ;
#54411=CARTESIAN_POINT ( 'NONE',  ( -20.97943885474387216, 2.004451313549292735, 11.49999999999999645 ) ) ;
#54412=CARTESIAN_POINT ( 'NONE',  ( 22.05266032001784637, -1.487345182339283367, 11.49999999999998934 ) ) ;
#54413=EDGE_CURVE ( 'NONE', #13115, #84470, #70275, .T. ) ;
#54414=CARTESIAN_POINT ( 'NONE',  ( -16.44861368136865920, 12.28130381464353782, -1.500000000000002220 ) ) ;
#54416=CARTESIAN_POINT ( 'NONE',  ( -60.54477366480123379, -24.40034930558990922, 0.3402023900116026289 ) ) ;
#54418=CARTESIAN_POINT ( 'NONE',  ( -32.62287095715004881, -24.64898659630367206, 1.056161002820817485 ) ) ;
#54419=ORIENTED_EDGE ( 'NONE', *, *, #90877, .T. ) ;
#54422=ORIENTED_EDGE ( 'NONE', *, *, #70611, .T. ) ;
#54424=ORIENTED_EDGE ( 'NONE', *, *, #7604, .F. ) ;
#54426=ORIENTED_EDGE ( 'NONE', *, *, #2502, .T. ) ;
#54427=CARTESIAN_POINT ( 'NONE',  ( -116.9228709571500389, -23.47593901973090169, -1.443836447538996648 ) ) ;
#54428=CARTESIAN_POINT ( 'NONE',  ( -74.62287095715004170, -24.66019654487199375, 8.947790411086129936 ) ) ;
#54429=CARTESIAN_POINT ( 'NONE',  ( -68.52210146834674731, -23.48786465467241058, 11.44779295918254824 ) ) ;
#54430=CARTESIAN_POINT ( 'NONE',  ( -18.82610421443283499, -8.410905081555696938, -1.500000000000002220 ) ) ;
#54432=CARTESIAN_POINT ( 'NONE',  ( -8.642975711230413083, 19.83371042614930957, 11.49999999999999645 ) ) ;
#54433=ORIENTED_EDGE ( 'NONE', *, *, #44990, .F. ) ;
#54436=CARTESIAN_POINT ( 'NONE',  ( -20.28323820415832657, -9.445149539555593776, -1.500000000000002220 ) ) ;
#54437=VECTOR ( 'NONE', #73005, 1000.000000000000114 ) ;
#54438=CARTESIAN_POINT ( 'NONE',  ( -71.52287095715006160, -24.34917612406836795, 0.1852690917426534634 ) ) ;
#54441=CARTESIAN_POINT ( 'NONE',  ( -117.0507892446735525, -25.34772161262076295, 6.200219024653767619 ) ) ;
#54443=CARTESIAN_POINT ( 'NONE',  ( 4.013313563623547964, -20.52093592976233438, -1.500000000000002220 ) ) ;
#54444=VERTEX_POINT ( 'NONE', #51115 ) ;
#54445=EDGE_CURVE ( 'NONE', #96748, #73913, #35250, .T. ) ;
#54447=ORIENTED_EDGE ( 'NONE', *, *, #4292, .F. ) ;
#54449=CARTESIAN_POINT ( 'NONE',  ( -6.202713861520617655, -20.23501359363181962, -1.500000000000002220 ) ) ;
#54450=ORIENTED_EDGE ( 'NONE', *, *, #71542, .F. ) ;
#54451=CARTESIAN_POINT ( 'NONE',  ( -50.58555295165667332, -24.63355581998386157, 0.9682620441943928791 ) ) ;
#54452=CARTESIAN_POINT ( 'NONE',  ( -9.857415191643349672, 19.42730305858377449, -1.500000000000002220 ) ) ;
#54453=CARTESIAN_POINT ( 'NONE',  ( -121.5228709571500616, -23.48786465467241769, 11.44779295918253759 ) ) ;
#54454=CARTESIAN_POINT ( 'NONE',  ( -41.52287095715006870, -23.47593901973090169, -1.443836447538997092 ) ) ;
#54455=CARTESIAN_POINT ( 'NONE',  ( -35.52287095715008292, -24.82576562948883137, 8.398263436605599708 ) ) ;
#54456=CARTESIAN_POINT ( 'NONE',  ( 18.19902423439809525, 11.99547645517801442, -1.500000000000002220 ) ) ;
#54457=CARTESIAN_POINT ( 'NONE',  ( -30.57287095715006586, -24.75921641729242495, 8.610803353223845491 ) ) ;
#54459=B_SPLINE_CURVE_WITH_KNOTS ( 'NONE', 3,
 ( #90306, #21771, #13663, #29399 ),
 .UNSPECIFIED., .F., .F.,
 ( 4, 4 ),
 ( 0.000000000000000000, 9.999999999997510880E-05 ),
 .UNSPECIFIED. ) ;
#54461=CARTESIAN_POINT ( 'NONE',  ( -117.5228709571500616, -24.50216790748203977, 0.6166512839542631630 ) ) ;
#54466=B_SPLINE_CURVE_WITH_KNOTS ( 'NONE', 3,
 ( #1741, #93566, #39789, #48422, #33181, #86965, #94581, #95582 ),
 .UNSPECIFIED., .F., .F.,
 ( 4, 2, 2, 4 ),
 ( 6.391158118975187985E-06, 0.002007136338672934825, 0.003007508928949912536, 0.004007881519226890246 ),
 .UNSPECIFIED. ) ;
#54467=CARTESIAN_POINT ( 'NONE',  ( -70.32380231474228083, -25.13313949306887096, 7.101635536975467566 ) ) ;
#54469=CARTESIAN_POINT ( 'NONE',  ( 0.06830352742921809439, -21.21198074455918814, -1.500000000000002220 ) ) ;
#54470=CARTESIAN_POINT ( 'NONE',  ( -52.62287095715005592, -24.66019654487199020, 8.947790411086135265 ) ) ;
#54471=CARTESIAN_POINT ( 'NONE',  ( -80.18401481691103072, -25.27791967176670340, 7.536602771734753681 ) ) ;
#54473=CARTESIAN_POINT ( 'NONE',  ( -48.52287095715006160, -23.47596703998600631, 11.44779298504229104 ) ) ;
#54474=CARTESIAN_POINT ( 'NONE',  ( 14.41255161864883583, -12.98630880007775268, 11.49999999999998934 ) ) ;
#54475=CARTESIAN_POINT ( 'NONE',  ( -41.88654540179980756, -25.30060000302003687, 6.009290021095885059 ) ) ;
#54476=ORIENTED_EDGE ( 'NONE', *, *, #68022, .T. ) ;
#54477=CARTESIAN_POINT ( 'NONE',  ( 1.255614643274026276, -19.41590359075080841, 11.49999999999999645 ) ) ;
#54479=EDGE_CURVE ( 'NONE', #35375, #32600, #40257, .T. ) ;
#54481=EDGE_LOOP ( 'NONE', ( #48839, #100366, #95048, #76676 ) ) ;
#54483=CARTESIAN_POINT ( 'NONE',  ( -97.52287095715010423, -23.48783264082477018, -1.443836473390087027 ) ) ;
#54484=CARTESIAN_POINT ( 'NONE',  ( -64.62287095715009855, -24.33832256527048088, 0.1851278514138592346 ) ) ;
#54486=CARTESIAN_POINT ( 'NONE',  ( 19.59260286812380514, -1.442238090573773501, -1.500000000000002220 ) ) ;
#54489=CARTESIAN_POINT ( 'NONE',  ( -16.60028029328060128, 13.79055755010687356, -1.500000000000002220 ) ) ;
#54490=CARTESIAN_POINT ( 'NONE',  ( -40.53727650475425293, -24.52300882791530157, 0.6510814631126360386 ) ) ;
#54492=CARTESIAN_POINT ( 'NONE',  ( -19.18584950847915493, -12.73052202388904952, -1.500000000000002220 ) ) ;
#54495=B_SPLINE_CURVE_WITH_KNOTS ( 'NONE', 3,
 ( #10038, #40998, #71955, #87669, #18149, #13893 ),
 .UNSPECIFIED., .F., .F.,
 ( 4, 2, 4 ),
 ( 1.570887131794795405E-05, 0.001396322306279765193, 0.002776935741241582344 ),
 .UNSPECIFIED. ) ;
#54497=CARTESIAN_POINT ( 'NONE',  ( -93.58859060503255023, -24.34968618360934300, 0.1864209137778838898 ) ) ;
#54498=CARTESIAN_POINT ( 'NONE',  ( -90.52287095715006160, -24.99156044556202616, 7.747789690856173195 ) ) ;
#54499=CARTESIAN_POINT ( 'NONE',  ( -121.6259261874522934, -23.96169478059713498, 10.65365249895717525 ) ) ;
#54501=VECTOR ( 'NONE', #20828, 1000.000000000000227 ) ;
#54503=CARTESIAN_POINT ( 'NONE',  ( -111.5321115232925564, -25.29823951520918612, 3.478177323284377120 ) ) ;
#54504=CARTESIAN_POINT ( 'NONE',  ( -129.5559603475894903, -23.96119346886880663, -0.6495511937831975890 ) ) ;
#54505=CARTESIAN_POINT ( 'NONE',  ( -114.6278463927332893, -23.96169478059714208, 10.65365249895717170 ) ) ;
#54506=CARTESIAN_POINT ( 'NONE',  ( 19.87125486832220744, 0.9792442318621276121, -1.500000000000002220 ) ) ;
#54508=CARTESIAN_POINT ( 'NONE',  ( -79.11611000704996854, -25.14083923594767001, 2.947789366383933185 ) ) ;
#54509=CARTESIAN_POINT ( 'NONE',  ( -2.602694502683683631, -19.63732897141692391, -1.500000000000002220 ) ) ;
#54510=VECTOR ( 'NONE', #44929, 1000.000000000000114 ) ;
#54514=CARTESIAN_POINT ( 'NONE',  ( -94.62287095715005592, -23.47593901973091235, -1.443836447539002865 ) ) ;
#54515=CARTESIAN_POINT ( 'NONE',  ( 20.29938135082171158, -4.300543036493735372, 11.49999999999999645 ) ) ;
#54518=CARTESIAN_POINT ( 'NONE',  ( -106.5515625499468371, -24.34968618360934300, 0.1864209137778878034 ) ) ;
#54519=CARTESIAN_POINT ( 'NONE',  ( -22.16177213047534877, -5.259615592301647879, 11.49999999999999645 ) ) ;
#54520=ORIENTED_EDGE ( 'NONE', *, *, #21002, .F. ) ;
#54521=CARTESIAN_POINT ( 'NONE',  ( -69.63097038022910112, -24.34968618360933945, 0.1864209137778826408 ) ) ;
#54522=CARTESIAN_POINT ( 'NONE',  ( -69.39531695424813051, -25.21178052097284450, 6.510839736813604617 ) ) ;
#54523=ORIENTED_EDGE ( 'NONE', *, *, #12664, .F. ) ;
#54524=CARTESIAN_POINT ( 'NONE',  ( -19.56588111578679090, -4.897929960003377658, -1.500000000000002220 ) ) ;
#54526=CARTESIAN_POINT ( 'NONE',  ( -97.62287095715008434, -23.47596703998600631, 11.44779298504227860 ) ) ;
#54530=CARTESIAN_POINT ( 'NONE',  ( 12.66508800429495629, 19.07499079241581086, -1.500000000000002220 ) ) ;
#54531=CARTESIAN_POINT ( 'NONE',  ( -51.10270014058699672, -25.18439706043954018, 3.552654129014596762 ) ) ;
#54532=CARTESIAN_POINT ( 'NONE',  ( -9.004746288917990782, -19.65190454534591069, -1.500000000000002220 ) ) ;
#54534=CARTESIAN_POINT ( 'NONE',  ( -13.97254113366623152, 15.51630364309664856, 11.49999999999999645 ) ) ;
#54535=ORIENTED_EDGE ( 'NONE', *, *, #50484, .T. ) ;
#54537=CARTESIAN_POINT ( 'NONE',  ( -21.12052157030387889, 6.262089831203976331, -1.500000000000002220 ) ) ;
#54539=CARTESIAN_POINT ( 'NONE',  ( -66.58953762381672448, -24.64965694238406968, 8.947790433994660120 ) ) ;
#54540=EDGE_CURVE ( 'NONE', #19866, #93563, #79305, .T. ) ;
#54543=PLANE ( 'NONE',  #28426 ) ;
#54544=ORIENTED_EDGE ( 'NONE', *, *, #80729, .F. ) ;
#54548=CARTESIAN_POINT ( 'NONE',  ( -71.56491059194962645, -23.48786465467241058, 11.44779295918254824 ) ) ;
#54551=CARTESIAN_POINT ( 'NONE',  ( 20.41236503877875563, 1.188189311754236144, -1.500000000000002220 ) ) ;
#54553=CARTESIAN_POINT ( 'NONE',  ( -79.52287095715009002, -24.33832256527049154, 0.1851278514138619824 ) ) ;
#54554=CARTESIAN_POINT ( 'NONE',  ( -44.62858516920130114, -24.51314013834316086, 0.6176544820404110681 ) ) ;
#54556=CARTESIAN_POINT ( 'NONE',  ( -13.27262489239681997, 17.90159134968837051, 11.49999999999998934 ) ) ;
#54558=CARTESIAN_POINT ( 'NONE',  ( -90.55620429048339304, -23.47593901973091235, -1.443836447539002865 ) ) ;
#54562=CARTESIAN_POINT ( 'NONE',  ( -29.81175120719462157, -24.63645345484493632, 4.942812314408664420 ) ) ;
#54563=CARTESIAN_POINT ( 'NONE',  ( -5.744250498300313090, 20.02623800365557472, -1.500000000000002220 ) ) ;
#54569=EDGE_LOOP ( 'NONE', ( #11501, #59815, #28161, #84846 ) ) ;
#54570=CARTESIAN_POINT ( 'NONE',  ( -51.11259392460791418, -25.12217823885073997, 6.923368740699049617 ) ) ;
#54571=CARTESIAN_POINT ( 'NONE',  ( 20.78037738254806399, 3.014218216234254566, -1.500000000000002220 ) ) ;
#54572=EDGE_CURVE ( 'NONE', #71695, #9907, #56996, .T. ) ;
#54574=AXIS2_PLACEMENT_3D ( 'NONE', #1656, #86879, #84875 ) ;
#54576=DIRECTION ( 'NONE',  ( -0.000000000000000000, 2.173523156925979552E-06, -0.9999999999976378895 ) ) ;
#54580=CARTESIAN_POINT ( 'NONE',  ( -92.62572372221266903, -24.51419770103156281, 9.386484678747175181 ) ) ;
#54582=CARTESIAN_POINT ( 'NONE',  ( -9.187330254778467875, -20.22999604658808082, 11.49999999999999645 ) ) ;
#54585=CARTESIAN_POINT ( 'NONE',  ( -93.62287095715005592, -24.64965695001468404, 8.947790433994180503 ) ) ;
#54587=CARTESIAN_POINT ( 'NONE',  ( -0.4833002549469566644, -22.66139224067150337, 11.49999999999998934 ) ) ;
#54589=VECTOR ( 'NONE', #8959, 1000.000000000000227 ) ;
#54590=EDGE_CURVE ( 'NONE', #77509, #26860, #87346, .T. ) ;
#54591=CARTESIAN_POINT ( 'NONE',  ( -111.5228709571500616, -24.35013146730204525, 9.818937971375092388 ) ) ;
#54592=ORIENTED_EDGE ( 'NONE', *, *, #1703, .T. ) ;
#54596=CARTESIAN_POINT ( 'NONE',  ( 14.76687977769557847, -13.71354340032049457, -1.500000000000002220 ) ) ;
#54599=DIRECTION ( 'NONE',  ( 3.773278334444167608E-23, -1.000000000000000000, 0.000000000000000000 ) ) ;
#54600=CARTESIAN_POINT ( 'NONE',  ( -12.45998644600372884, -18.51849504856558681, -1.500000000000002220 ) ) ;
#54601=EDGE_CURVE ( 'NONE', #69272, #98613, #23174, .T. ) ;
#54605=CARTESIAN_POINT ( 'NONE',  ( -94.50776865740360222, -24.51419770103156281, 9.386484678747184063 ) ) ;
#54608=DIRECTION ( 'NONE',  ( -3.773278334444166432E-23, 1.000000000000000000, 0.000000000000000000 ) ) ;
#54610=CARTESIAN_POINT ( 'NONE',  ( 19.54226456527178257, 0.3027743077981833730, 11.49999999999998934 ) ) ;
#54612=CARTESIAN_POINT ( 'NONE',  ( 4.199879391047538491, -21.09745483596041282, 11.49999999999998934 ) ) ;
#54614=FACE_OUTER_BOUND ( 'NONE', #7567, .T. ) ;
#54615=CARTESIAN_POINT ( 'NONE',  ( -50.40445135320380388, -25.18492896333868103, 3.293943116708552221 ) ) ;
#54616=DIRECTION ( 'NONE',  ( 1.000000000000000000, 3.773278334444166432E-23, 8.201307841325785021E-29 ) ) ;
#54618=CARTESIAN_POINT ( 'NONE',  ( -20.40978113611479827, 10.34812579263477872, -1.500000000000002220 ) ) ;
#54619=EDGE_CURVE ( 'NONE', #50558, #58657, #59505, .T. ) ;
#54620=B_SPLINE_CURVE_WITH_KNOTS ( 'NONE', 3,
 ( #15648, #70953, #69937, #425 ),
 .UNSPECIFIED., .F., .F.,
 ( 4, 4 ),
 ( 0.000000000000000000, 0.0001000000000000167422 ),
 .UNSPECIFIED. ) ;
#54621=EDGE_CURVE ( 'NONE', #91381, #77509, #49625, .T. ) ;
#54624=CARTESIAN_POINT ( 'NONE',  ( -53.56013271601442227, -23.73766607897669800, -1.055555164236460008 ) ) ;
#54625=CARTESIAN_POINT ( 'NONE',  ( -19.89792590360708147, -2.209704250470923892, 11.49999999999999645 ) ) ;
#54626=CARTESIAN_POINT ( 'NONE',  ( -78.96619831399281964, -25.26612626921278348, 5.670633042279167313 ) ) ;
#54628=CARTESIAN_POINT ( 'NONE',  ( -78.52287095715006160, -29.50250243563736774, 8.947779886222141599 ) ) ;
#54629=LINE ( 'NONE', #79453, #53746 ) ;
#54630=ORIENTED_EDGE ( 'NONE', *, *, #74495, .F. ) ;
#54631=CARTESIAN_POINT ( 'NONE',  ( -50.62287095715005592, -24.83620972994591014, 8.398175272781365663 ) ) ;
#54632=CARTESIAN_POINT ( 'NONE',  ( -115.6228709571500843, -24.92604778743018201, 8.074972756849350120 ) ) ;
#54633=EDGE_CURVE ( 'NONE', #67086, #90447, #8447, .T. ) ;
#54634=CARTESIAN_POINT ( 'NONE',  ( 9.899741330608472722, -19.37759744025533593, -1.500000000000002220 ) ) ;
#54635=CARTESIAN_POINT ( 'NONE',  ( -19.61143073682725202, -1.510137823221562092, -1.500000000000002220 ) ) ;
#54637=PLANE ( 'NONE',  #52377 ) ;
#54638=EDGE_CURVE ( 'NONE', #37940, #73668, #65618, .T. ) ;
#54640=DIRECTION ( 'NONE',  ( 1.000000000000000000, 3.773278334444166432E-23, 8.201307841325785021E-29 ) ) ;
#54644=CARTESIAN_POINT ( 'NONE',  ( 10.47388184937329214, 17.72644800832989986, 11.49999999999999645 ) ) ;
#54649=VERTEX_POINT ( 'NONE', #3702 ) ;
#54650=CARTESIAN_POINT ( 'NONE',  ( -100.3574794290996266, -25.26387448364017985, 4.711073633588144460 ) ) ;
#54652=CARTESIAN_POINT ( 'NONE',  ( -108.5562042904834072, -23.48783264082479505, -1.443836473390060160 ) ) ;
#54655=CARTESIAN_POINT ( 'NONE',  ( -33.62287095715005592, -23.72747288104469732, -1.053458166803227680 ) ) ;
#54656=CARTESIAN_POINT ( 'NONE',  ( -42.62287095715005592, -23.95044443724992078, 10.65354141964649592 ) ) ;
#54657=B_SPLINE_CURVE_WITH_KNOTS ( 'NONE', 3,
 ( #78756, #23978, #47836, #40220 ),
 .UNSPECIFIED., .F., .F.,
 ( 4, 4 ),
 ( 0.000000000000000000, 9.999999999996123101E-05 ),
 .UNSPECIFIED. ) ;
#54658=EDGE_LOOP ( 'NONE', ( #60597, #57064, #94059, #74148 ) ) ;
#54659=CARTESIAN_POINT ( 'NONE',  ( 22.92345266703080142, -2.467471440992916154, 11.49999999999999645 ) ) ;
#54660=CARTESIAN_POINT ( 'NONE',  ( 17.58993269669914383, -14.52173041563253975, 11.49999999999998934 ) ) ;
#54662=CARTESIAN_POINT ( 'NONE',  ( -96.63573453449330941, -23.73766607897670511, -1.055555164236452681 ) ) ;
#54664=B_SPLINE_CURVE_WITH_KNOTS ( 'NONE', 3,
 ( #99881, #59862, #91294, #46634, #99398, #30389 ),
 .UNSPECIFIED., .F., .F.,
 ( 4, 2, 4 ),
 ( 0.000000000000000000, 0.001380901958385385509, 0.002761803916770771018 ),
 .UNSPECIFIED. ) ;
#54665=CARTESIAN_POINT ( 'NONE',  ( 17.77913403553526805, 13.70458096452923691, 11.49999999999999645 ) ) ;
#54667=CARTESIAN_POINT ( 'NONE',  ( -69.62287095715005592, -24.65952944569304961, 1.056160979905697017 ) ) ;
#54668=CARTESIAN_POINT ( 'NONE',  ( -70.62287095715004170, -24.52323809116983355, 9.355190652339413049 ) ) ;
#54669=CARTESIAN_POINT ( 'NONE',  ( 5.197331492371871420, 21.31670716312865466, 11.49999999999998934 ) ) ;
#54671=CARTESIAN_POINT ( 'NONE',  ( -34.47819092748605385, -24.66019654487199730, 8.947790411086117501 ) ) ;
#54673=VERTEX_POINT ( 'NONE', #12785 ) ;
#54675=DIRECTION ( 'NONE',  ( 0.000000000000000000, -2.173523156925979552E-06, 0.9999999999976378895 ) ) ;
#54677=CARTESIAN_POINT ( 'NONE',  ( -12.04554601739387998, 16.56303510970703385, 11.49999999999998934 ) ) ;
#54680=ORIENTED_EDGE ( 'NONE', *, *, #75756, .F. ) ;
#54682=CARTESIAN_POINT ( 'NONE',  ( 0.1381291366035634904, -23.06709338131901532, -1.500000000000002220 ) ) ;
#54683=CARTESIAN_POINT ( 'NONE',  ( -49.28099472632571576, -25.20958802453461089, 3.393435110817564215 ) ) ;
#54684=CARTESIAN_POINT ( 'NONE',  ( -11.07518157712430096, -17.02944518001645946, -1.500000000000002220 ) ) ;
#54685=VERTEX_POINT ( 'NONE', #27029 ) ;
#54688=CARTESIAN_POINT ( 'NONE',  ( -92.63100931479979749, -24.15543982623908192, -0.2315651400026453588 ) ) ;
#54689=CARTESIAN_POINT ( 'NONE',  ( -28.52287095715006870, -23.78764107635717906, 10.65372851796821685 ) ) ;
#54691=CARTESIAN_POINT ( 'NONE',  ( -18.46100929034391314, -11.06139713797464985, 11.49999999999999645 ) ) ;
#54693=CARTESIAN_POINT ( 'NONE',  ( -75.63387239539466123, -24.52300882791530512, 0.6510814631126415897 ) ) ;
#54694=CARTESIAN_POINT ( 'NONE',  ( -94.62287095715005592, -24.64965695001469115, 8.947790433994180503 ) ) ;
#54697=CARTESIAN_POINT ( 'NONE',  ( -17.23291202157775359, 11.51834372740795231, 11.49999999999998934 ) ) ;
#54698=ORIENTED_EDGE ( 'NONE', *, *, #49595, .T. ) ;
#54699=CARTESIAN_POINT ( 'NONE',  ( -69.86226847989213695, -25.12049686670126292, 2.832401160916445004 ) ) ;
#54700=ORIENTED_EDGE ( 'NONE', *, *, #89084, .F. ) ;
#54704=CARTESIAN_POINT ( 'NONE',  ( -111.6272348879597587, -24.15620529776629510, 10.23563542870659582 ) ) ;
#54705=LINE ( 'NONE', #71427, #50289 ) ;
#54706=ORIENTED_EDGE ( 'NONE', *, *, #5546, .T. ) ;
#54707=VERTEX_POINT ( 'NONE', #57499 ) ;
#54708=ADVANCED_FACE ( 'NONE', ( #58492 ), #19900, .T. ) ;
#54709=DIRECTION ( 'NONE',  ( 1.000000000000000000, 3.773278334444167608E-23, 8.201307833595939069E-29 ) ) ;
#54710=CARTESIAN_POINT ( 'NONE',  ( -42.64759707562362934, -23.96169478059713143, 10.65365249895718947 ) ) ;
#54711=CARTESIAN_POINT ( 'NONE',  ( -102.5228709571500332, -23.95044443724990657, 10.65354141964648882 ) ) ;
#54712=CARTESIAN_POINT ( 'NONE',  ( -2.902263480631018577, 21.84654903556016947, 11.49999999999999645 ) ) ;
#54713=EDGE_CURVE ( 'NONE', #17843, #76499, #4856, .T. ) ;
#54714=CARTESIAN_POINT ( 'NONE',  ( -89.63470426873689689, -23.96169478059713498, 10.65365249895717703 ) ) ;
#54715=CARTESIAN_POINT ( 'NONE',  ( 22.38532167473930556, -2.757513164441831144, -1.500000000000002220 ) ) ;
#54717=AXIS2_PLACEMENT_3D ( 'NONE', #80937, #83797, #36628 ) ;
#54718=CARTESIAN_POINT ( 'NONE',  ( -2.639205680565387624, -20.84613592336672028, 11.49999999999998934 ) ) ;
#54721=VERTEX_POINT ( 'NONE', #52364 ) ;
#54725=CARTESIAN_POINT ( 'NONE',  ( -113.6228709571500417, -24.50321055353806088, 9.387540953477516936 ) ) ;
#54727=CARTESIAN_POINT ( 'NONE',  ( -1.424071398598787397, -21.11453822904667277, 11.49999999999998934 ) ) ;
#54728=CARTESIAN_POINT ( 'NONE',  ( -83.62287095715005592, -24.64898659630528854, 1.056161002820826145 ) ) ;
#54729=CARTESIAN_POINT ( 'NONE',  ( -51.78109907783319699, -25.26040949718250772, 6.793045023519886705 ) ) ;
#54730=CARTESIAN_POINT ( 'NONE',  ( -49.71071415242499114, -25.29402636989360076, 4.468221159579485402 ) ) ;
#54732=CARTESIAN_POINT ( 'NONE',  ( -44.52287095715006160, -29.50247984919015209, -1.443849546365060466 ) ) ;
#54733=DIRECTION ( 'NONE',  ( -3.773278334453079618E-23, 0.9999999999976377785, 2.173523156925979975E-06 ) ) ;
#54734=CARTESIAN_POINT ( 'NONE',  ( -14.74362065938029076, 16.57599527146691898, -1.500000000000002220 ) ) ;
#54735=CARTESIAN_POINT ( 'NONE',  ( -71.60770107105075510, -23.48783264082476663, -1.443836473390092578 ) ) ;
#54736=EDGE_CURVE ( 'NONE', #28349, #73864, #67770, .T. ) ;
#54739=CARTESIAN_POINT ( 'NONE',  ( -48.62287095715004881, -23.94994826722515313, -0.6494450866351707541 ) ) ;
#54740=CARTESIAN_POINT ( 'NONE',  ( -126.6237062192220861, -24.51314013834316796, 0.6176544820404223923 ) ) ;
#54741=CARTESIAN_POINT ( 'NONE',  ( -100.5044705759059269, -25.00158670708910691, 2.256160236439218369 ) ) ;
#54743=EDGE_CURVE ( 'NONE', #12190, #68328, #21726, .T. ) ;
#54744=CARTESIAN_POINT ( 'NONE',  ( 18.22972481837485859, -6.773019484731225504, 11.49999999999998934 ) ) ;
#54745=B_SPLINE_CURVE_WITH_KNOTS ( 'NONE', 3,
 ( #55324, #78622, #17749, #32471 ),
 .UNSPECIFIED., .F., .F.,
 ( 4, 4 ),
 ( 0.000000000000000000, 9.999999999998206125E-05 ),
 .UNSPECIFIED. ) ;
#54746=CARTESIAN_POINT ( 'NONE',  ( 20.74164082462262471, 5.259929546262127609, 11.49999999999998934 ) ) ;
#54747=CARTESIAN_POINT ( 'NONE',  ( -68.94187076657172497, -25.24898040475824246, 6.277239383255088789 ) ) ;
#54748=CARTESIAN_POINT ( 'NONE',  ( -94.52287095715006160, -24.64965694238575011, 8.947790433994196491 ) ) ;
#54750=CARTESIAN_POINT ( 'NONE',  ( -101.1478676400630405, -25.27360041239775512, 3.600571350085281175 ) ) ;
#54751=CARTESIAN_POINT ( 'NONE',  ( -14.94938274637043207, -17.11189489004485864, -1.500000000000002220 ) ) ;
#54752=EDGE_CURVE ( 'NONE', #84710, #28719, #26602, .T. ) ;
#54753=CARTESIAN_POINT ( 'NONE',  ( -98.55492856983048000, -23.96119346886880663, -0.6495511937832080251 ) ) ;
#54755=CARTESIAN_POINT ( 'NONE',  ( -19.55781625546462976, 3.520333346782119843, 11.49999999999999645 ) ) ;
#54756=CARTESIAN_POINT ( 'NONE',  ( -123.5546973089963956, -24.35071581493544457, 9.817618358456016381 ) ) ;
#54757=CARTESIAN_POINT ( 'NONE',  ( -32.52287095715006160, -23.48783264083359867, -1.443836473376375329 ) ) ;
#54761=CARTESIAN_POINT ( 'NONE',  ( -117.5562042904833930, -24.66019654487199730, 8.947790411086121054 ) ) ;
#54762=CARTESIAN_POINT ( 'NONE',  ( -10.04279811845843007, 19.21892966915218892, -1.500000000000002220 ) ) ;
#54765=CARTESIAN_POINT ( 'NONE',  ( 5.650214204171827070, -18.61605495904187535, -1.500000000000002220 ) ) ;
#54766=DIRECTION ( 'NONE',  ( -3.773278334444167608E-23, 1.000000000000000000, 0.000000000000000000 ) ) ;
#54768=B_SPLINE_CURVE_WITH_KNOTS ( 'NONE', 3,
 ( #73327, #40371, #65239, #64742, #34758, #26649 ),
 .UNSPECIFIED., .F., .F.,
 ( 4, 2, 4 ),
 ( 1.570755371633797249E-05, 0.001396183895866087319, 0.002776660238015836446 ),
 .UNSPECIFIED. ) ;
#54769=ORIENTED_EDGE ( 'NONE', *, *, #19531, .F. ) ;
#54770=CARTESIAN_POINT ( 'NONE',  ( 18.82465703714932204, -7.861812626244089053, 11.49999999999999645 ) ) ;
#54771=DIRECTION ( 'NONE',  ( -3.773278334453080206E-23, 0.9999999999976377785, 2.173523156925979975E-06 ) ) ;
#54772=EDGE_CURVE ( 'NONE', #20834, #84257, #90862, .T. ) ;
#54774=ORIENTED_EDGE ( 'NONE', *, *, #25474, .F. ) ;
#54775=CARTESIAN_POINT ( 'NONE',  ( -40.70660919605776940, -25.19832496394808885, 3.317317603583394892 ) ) ;
#54776=CARTESIAN_POINT ( 'NONE',  ( -92.52287095715006160, -23.94994826722565762, -0.6494450866342746931 ) ) ;
#54777=LINE ( 'NONE', #61890, #56486 ) ;
#54778=CARTESIAN_POINT ( 'NONE',  ( -40.57216639332711594, -25.00182538069146787, 7.747789668545040698 ) ) ;
#54779=DIRECTION ( 'NONE',  ( 1.000000000000000000, 3.773278334444166432E-23, 8.201307841325785021E-29 ) ) ;
#54780=CARTESIAN_POINT ( 'NONE',  ( 1.236116150138429903, -20.07036509671028668, 11.49999999999998934 ) ) ;
#54781=EDGE_CURVE ( 'NONE', #78854, #50194, #37629, .T. ) ;
#54783=ORIENTED_EDGE ( 'NONE', *, *, #65772, .F. ) ;
#54784=CARTESIAN_POINT ( 'NONE',  ( -82.22287095715006444, -23.47593901973090169, -1.443836447538997092 ) ) ;
#54786=CARTESIAN_POINT ( 'NONE',  ( 6.305670413343573699, 22.00876638805999974, 11.49999999999999645 ) ) ;
#54787=CARTESIAN_POINT ( 'NONE',  ( -20.26579564662877075, -10.28286414166031726, 11.49999999999998934 ) ) ;
#54789=CARTESIAN_POINT ( 'NONE',  ( -71.66738459694697383, -25.21749834187382078, 6.546833690950035312 ) ) ;
#54790=LINE ( 'NONE', #78093, #99591 ) ;
#54791=LINE ( 'NONE', #54294, #85692 ) ;
#54792=CARTESIAN_POINT ( 'NONE',  ( -30.57287095715006586, -23.79279866861233828, 10.96694982589930767 ) ) ;
#54793=VECTOR ( 'NONE', #97970, 1000.000000000000114 ) ;
#54794=CARTESIAN_POINT ( 'NONE',  ( -118.6228709571500701, -23.48786465467241769, 11.44779295918253759 ) ) ;
#54795=CARTESIAN_POINT ( 'NONE',  ( -98.90869474253671001, -25.31200697284943146, 5.895134381143665614 ) ) ;
#54796=ORIENTED_EDGE ( 'NONE', *, *, #2639, .T. ) ;
#54797=VECTOR ( 'NONE', #63518, 1000.000000000000114 ) ;
#54798=CARTESIAN_POINT ( 'NONE',  ( -13.40315722217803973, 15.35114911505495172, -1.500000000000002220 ) ) ;
#54799=ORIENTED_EDGE ( 'NONE', *, *, #14674, .F. ) ;
#54800=CARTESIAN_POINT ( 'NONE',  ( 4.903590608199674072, 22.46510890469962263, -1.500000000000002220 ) ) ;
#54801=DIRECTION ( 'NONE',  ( 1.000000000000000000, 3.773278334444166432E-23, 8.201307841325785021E-29 ) ) ;
#54803=CARTESIAN_POINT ( 'NONE',  ( -108.6314038554107100, -23.73791477778912196, 11.05961554403169878 ) ) ;
#54805=CARTESIAN_POINT ( 'NONE',  ( -89.55620429048340725, -24.65952944569304606, 1.056160979905701014 ) ) ;
#54806=AXIS2_PLACEMENT_3D ( 'NONE', #73232, #17431, #27051 ) ;
#54807=CARTESIAN_POINT ( 'NONE',  ( 3.065528897535349628, -21.08962430476942274, 11.49999999999999645 ) ) ;
#54810=CARTESIAN_POINT ( 'NONE',  ( 21.63176498729014341, 4.993826359924048219, -1.500000000000002220 ) ) ;
#54811=CARTESIAN_POINT ( 'NONE',  ( 14.37238272058661259, 14.81585024043302035, 11.49999999999998934 ) ) ;
#54812=B_SPLINE_CURVE_WITH_KNOTS ( 'NONE', 3,
 ( #12513, #43480, #19624, #88155, #66830, #35369 ),
 .UNSPECIFIED., .F., .F.,
 ( 4, 2, 4 ),
 ( 1.570755371634033063E-05, 0.001396183895866089488, 0.002776660238015838614 ),
 .UNSPECIFIED. ) ;
#54813=ORIENTED_EDGE ( 'NONE', *, *, #95128, .F. ) ;
#54814=ORIENTED_EDGE ( 'NONE', *, *, #15652, .F. ) ;
#54815=CARTESIAN_POINT ( 'NONE',  ( -108.9979829822171951, -25.27682655912521881, 4.539662868468415269 ) ) ;
#54817=CARTESIAN_POINT ( 'NONE',  ( -95.62462548333338930, -24.92592662359561473, 8.075495903017998245 ) ) ;
#54819=EDGE_CURVE ( 'NONE', #66922, #17140, #22385, .T. ) ;
#54820=CARTESIAN_POINT ( 'NONE',  ( -50.40445135320378967, -25.13313949306887451, 7.101635536975466678 ) ) ;
#54821=EDGE_LOOP ( 'NONE', ( #70989, #17643, #85359, #71544 ) ) ;
#54822=CARTESIAN_POINT ( 'NONE',  ( -58.54268383830879685, -24.35071581493543036, 9.817618358456028815 ) ) ;
#54823=ADVANCED_FACE ( 'NONE', ( #60981 ), #61482, .T. ) ;
#54824=PLANE ( 'NONE',  #29268 ) ;
#54825=CARTESIAN_POINT ( 'NONE',  ( -17.75621389795859884, -10.86975384844714831, -1.500000000000002220 ) ) ;
#54826=CARTESIAN_POINT ( 'NONE',  ( 19.17057494584436839, 10.47865234463220396, 11.49999999999999645 ) ) ;
#54828=FACE_OUTER_BOUND ( 'NONE', #99495, .T. ) ;
#54829=CARTESIAN_POINT ( 'NONE',  ( -78.54638029082808259, -24.35071581493543391, 9.817618358456027039 ) ) ;
#54830=CARTESIAN_POINT ( 'NONE',  ( 19.77452139984142221, -10.64395493966388706, -1.500000000000002220 ) ) ;
#54832=CARTESIAN_POINT ( 'NONE',  ( -38.64868663285562178, -23.96119346886880308, -0.6495511937831990323 ) ) ;
#54833=CARTESIAN_POINT ( 'NONE',  ( -87.58953762381671027, -23.48783264082478794, -1.443836473390063269 ) ) ;
#54835=B_SPLINE_SURFACE_WITH_KNOTS ( 'NONE', 3, 3, ( 
 ( #55851, #47730, #541, #95398 ),
 ( #78646, #79664, #8662, #31489 ),
 ( #41122, #93380, #10163, #25382 ),
 ( #62453, #2066, #85785, #25887 ),
 ( #16267, #63980, #9152, #94393 ),
 ( #17270, #56859, #11159, #82167 ),
 ( #19753, #3064, #50729, #57857 ),
 ( #18763, #5044, #51224, #34004 ),
 ( #12651, #81674, #96396, #12147 ),
 ( #88797, #43117, #42627, #4055 ) ),
 .UNSPECIFIED., .F., .F., .F.,
 ( 4, 3, 3, 4 ),
 ( 4, 4 ),
 ( 0.7022005934544806038, 0.7765311282028796169, 0.8508616629512786300, 0.9995227324480766562 ),
 ( 0.7995904963587343595, 0.8010797657131805138 ),
 .UNSPECIFIED. ) ;
#54837=ORIENTED_EDGE ( 'NONE', *, *, #85735, .T. ) ;
#54839=CARTESIAN_POINT ( 'NONE',  ( -20.23222619987061677, -6.887663580918623296, -1.500000000000002220 ) ) ;
#54840=ORIENTED_EDGE ( 'NONE', *, *, #70466, .F. ) ;
#54841=CARTESIAN_POINT ( 'NONE',  ( -20.88184962559319402, -2.832954952542597660, 11.49999999999998934 ) ) ;
#54842=CARTESIAN_POINT ( 'NONE',  ( -30.46019145506044623, -23.77870465984290149, -0.9707498849204322378 ) ) ;
#54843=CARTESIAN_POINT ( 'NONE',  ( -11.44242300287478820, -16.35863574123370512, -1.500000000000002220 ) ) ;
#54845=CARTESIAN_POINT ( 'NONE',  ( -50.40895856474225667, -25.04307398257883577, 7.563174194274489892 ) ) ;
#54846=CARTESIAN_POINT ( 'NONE',  ( -12.87221125579857528, -17.80329210173279364, -1.500000000000002220 ) ) ;
#54847=PLANE ( 'NONE',  #73920 ) ;
#54849=CARTESIAN_POINT ( 'NONE',  ( -111.5228709571500616, -29.50250243563736774, 8.947779886222136270 ) ) ;
#54851=CARTESIAN_POINT ( 'NONE',  ( -121.5228709571500048, -23.47593901973090524, -1.443836447538996204 ) ) ;
#54852=CARTESIAN_POINT ( 'NONE',  ( -5.744250498300313090, 20.02623800365557472, 11.49999999999999645 ) ) ;
#54853=VECTOR ( 'NONE', #80589, 1000.000000000000227 ) ;
#54854=B_SPLINE_CURVE_WITH_KNOTS ( 'NONE', 3,
 ( #75897, #74897, #29732, #75396, #82518, #4907 ),
 .UNSPECIFIED., .F., .F.,
 ( 4, 2, 4 ),
 ( 0.000000000000000000, 0.001380901958385387027, 0.002761803916770774053 ),
 .UNSPECIFIED. ) ;
#54857=CARTESIAN_POINT ( 'NONE',  ( -38.62287095715004881, -23.96177878511306503, 10.65340807706330395 ) ) ;
#54858=CARTESIAN_POINT ( 'NONE',  ( -20.61954105445765251, -5.431428859615135885, 11.49999999999998934 ) ) ;
#54859=CARTESIAN_POINT ( 'NONE',  ( -98.52218354524907795, -23.48786465467241769, 11.44779295918254469 ) ) ;
#54860=DIRECTION ( 'NONE',  ( -3.773278334453079618E-23, 0.9999999999976377785, 2.173523156925979975E-06 ) ) ;
#54863=CARTESIAN_POINT ( 'NONE',  ( -3.310667818835141940, 22.29536907041311977, -1.500000000000002220 ) ) ;
#54864=CARTESIAN_POINT ( 'NONE',  ( -129.6228709571500417, -24.66019654487200086, 8.947790411086117501 ) ) ;
#54865=ORIENTED_EDGE ( 'NONE', *, *, #65397, .F. ) ;
#54866=CARTESIAN_POINT ( 'NONE',  ( -51.26855917001611829, -25.30346314791453821, 5.552786049883900787 ) ) ;
#54868=CARTESIAN_POINT ( 'NONE',  ( -13.08164486973500118, 14.69858247433046650, 11.49999999999999645 ) ) ;
#54869=FACE_OUTER_BOUND ( 'NONE', #52138, .T. ) ;
#54870=VECTOR ( 'NONE', #85968, 1000.000000000000114 ) ;
#54872=ORIENTED_EDGE ( 'NONE', *, *, #18656, .T. ) ;
#54873=DIRECTION ( 'NONE',  ( -1.000000000000000000, -3.773278334444165844E-23, -8.201307836089272790E-29 ) ) ;
#54877=CARTESIAN_POINT ( 'NONE',  ( 3.553741186906278493, -19.43417129498564577, -1.500000000000002220 ) ) ;
#54879=VERTEX_POINT ( 'NONE', #37131 ) ;
#54880=CARTESIAN_POINT ( 'NONE',  ( -120.5228709571500900, -25.00182538069145366, 7.747789668545101982 ) ) ;
#54881=EDGE_CURVE ( 'NONE', #29962, #32572, #37560, .T. ) ;
#54885=PLANE ( 'NONE',  #69402 ) ;
#54886=CARTESIAN_POINT ( 'NONE',  ( -53.62287095715005592, -24.64898659630528499, 1.056161002820821038 ) ) ;
#54888=CARTESIAN_POINT ( 'NONE',  ( -98.89303308397303738, -25.03144863224170180, 6.110950661846722198 ) ) ;
#54890=B_SPLINE_CURVE_WITH_KNOTS ( 'NONE', 3,
 ( #67355, #98275, #99280, #28781, #43019, #90677 ),
 .UNSPECIFIED., .F., .F.,
 ( 4, 2, 4 ),
 ( 0.000000000000000000, 0.001380764517854760195, 0.002761529035709520390 ),
 .UNSPECIFIED. ) ;
#54893=CARTESIAN_POINT ( 'NONE',  ( -18.81269933604069067, 6.858547123926768130, 11.49999999999998934 ) ) ;
#54894=CARTESIAN_POINT ( 'NONE',  ( -117.5228709571500758, -24.64898659630368272, 1.056161002820833028 ) ) ;
#54895=FACE_OUTER_BOUND ( 'NONE', #53433, .T. ) ;
#54897=CARTESIAN_POINT ( 'NONE',  ( -79.50884703881661153, -24.15620529776628089, 10.23563542870660470 ) ) ;
#54898=CARTESIAN_POINT ( 'NONE',  ( -109.3608459871604026, -25.29012903889914554, 4.114984869304729287 ) ) ;
#54899=CARTESIAN_POINT ( 'NONE',  ( -58.52287095715006870, -24.35013146730203815, 9.818937971375103047 ) ) ;
#54900=CARTESIAN_POINT ( 'NONE',  ( -101.5468792378191836, -25.25287247409163527, 6.236250661346386615 ) ) ;
#54901=CARTESIAN_POINT ( 'NONE',  ( -117.5801350442859672, -25.31825869351653679, 3.539998670762450672 ) ) ;
#54903=FACE_OUTER_BOUND ( 'NONE', #96277, .T. ) ;
#54904=LINE ( 'NONE', #78218, #37169 ) ;
#54906=AXIS2_PLACEMENT_3D ( 'NONE', #86286, #40118, #15767 ) ;
#54907=CARTESIAN_POINT ( 'NONE',  ( 6.844040470191356640, -19.11863935190610064, -1.500000000000002220 ) ) ;
#54909=AXIS2_PLACEMENT_3D ( 'NONE', #30214, #75890, #6391 ) ;
#54910=LINE ( 'NONE', #85853, #70313 ) ;
#54912=EDGE_CURVE ( 'NONE', #27060, #73557, #87169, .T. ) ;
#54914=CARTESIAN_POINT ( 'NONE',  ( -12.46103870137906711, 15.87156016069071462, -1.500000000000002220 ) ) ;
#54915=CARTESIAN_POINT ( 'NONE',  ( -15.95541298346445735, 13.85296639876547076, 11.49999999999999645 ) ) ;
#54917=CARTESIAN_POINT ( 'NONE',  ( 14.84500176111689207, -16.38379996218902335, 11.49999999999998934 ) ) ;
#54918=CARTESIAN_POINT ( 'NONE',  ( 4.814550503181614260, -19.98661186389175271, -1.500000000000002220 ) ) ;
#54919=CARTESIAN_POINT ( 'NONE',  ( -60.60739371882706195, -23.85016227208579664, -0.8807180028928355275 ) ) ;
#54920=ORIENTED_EDGE ( 'NONE', *, *, #12563, .F. ) ;
#54921=CARTESIAN_POINT ( 'NONE',  ( -32.62287095715007013, -23.94994826722565406, -0.6494450866342722506 ) ) ;
#54923=CARTESIAN_POINT ( 'NONE',  ( -51.62287095715006302, -24.33832256527048088, 0.1851278514138594566 ) ) ;
#54924=CARTESIAN_POINT ( 'NONE',  ( -70.52287095715010423, -23.84081130425358097, 10.88220057483159664 ) ) ;
#54925=EDGE_LOOP ( 'NONE', ( #20818, #59839, #71153, #56117 ) ) ;
#54926=EDGE_CURVE ( 'NONE', #65683, #44226, #50874, .T. ) ;
#54927=ORIENTED_EDGE ( 'NONE', *, *, #6045, .T. ) ;
#54931=CARTESIAN_POINT ( 'NONE',  ( -113.5228709571500616, -29.50247984919015209, -1.443849546365048253 ) ) ;
#54933=CARTESIAN_POINT ( 'NONE',  ( -6.358105417860958397, -19.66046682221446318, -1.500000000000002220 ) ) ;
#54934=CARTESIAN_POINT ( 'NONE',  ( 4.495418090846292181, 21.21921847905042569, 11.49999999999999645 ) ) ;
#54936=EDGE_CURVE ( 'NONE', #18736, #32470, #35056, .T. ) ;
#54939=CARTESIAN_POINT ( 'NONE',  ( -19.80502325505778671, 10.42642913751328670, 11.49999999999998934 ) ) ;
#54941=CARTESIAN_POINT ( 'NONE',  ( -79.42863770186421846, -25.12205661262295919, 6.408999591950016672 ) ) ;
#54942=CARTESIAN_POINT ( 'NONE',  ( -120.6228709571499706, -24.82576562982392687, 8.398263435472960836 ) ) ;
#54943=ORIENTED_EDGE ( 'NONE', *, *, #66528, .F. ) ;
#54944=B_SPLINE_CURVE_WITH_KNOTS ( 'NONE', 3,
 ( #4797, #50473, #75290, #34748 ),
 .UNSPECIFIED., .F., .F.,
 ( 4, 4 ),
 ( 0.000000000000000000, 9.999999999998897304E-05 ),
 .UNSPECIFIED. ) ;
#54946=CARTESIAN_POINT ( 'NONE',  ( -35.54073533905776827, -24.40133493613049609, 9.663955038902800609 ) ) ;
#54947=ADVANCED_FACE ( 'NONE', ( #33029 ), #46753, .F. ) ;
#54948=CARTESIAN_POINT ( 'NONE',  ( 8.587038044527741221, -19.06309208085484386, -1.500000000000002220 ) ) ;
#54953=CARTESIAN_POINT ( 'NONE',  ( -50.62287095715008434, -24.51254535404256529, 9.355368623467660072 ) ) ;
#54954=CARTESIAN_POINT ( 'NONE',  ( 8.100108036306837178, -19.54698220168213041, -1.500000000000002220 ) ) ;
#54956=CARTESIAN_POINT ( 'NONE',  ( -118.5228709571500758, -29.50248528299804818, 1.056150453629045360 ) ) ;
#54957=CARTESIAN_POINT ( 'NONE',  ( -21.44618410820073606, 4.064364382921047181, -1.500000000000002220 ) ) ;
#54960=CARTESIAN_POINT ( 'NONE',  ( -40.41683116089613748, -25.31532428806244539, 5.082404371757057504 ) ) ;
#54961=CARTESIAN_POINT ( 'NONE',  ( 9.495391690522565042, 19.61495305411445500, -1.500000000000002220 ) ) ;
#54962=CARTESIAN_POINT ( 'NONE',  ( -67.22287095715005023, -23.47593901973090169, -1.443836447538997536 ) ) ;
#54963=ORIENTED_EDGE ( 'NONE', *, *, #26779, .F. ) ;
#54965=CARTESIAN_POINT ( 'NONE',  ( -30.57287095715006942, -23.48213395187224606, 11.44779283644488999 ) ) ;
#54966=CARTESIAN_POINT ( 'NONE',  ( -85.50024737997124191, -24.73531770709095312, 8.716586749053508498 ) ) ;
#54967=ORIENTED_EDGE ( 'NONE', *, *, #76438, .F. ) ;
#54968=ORIENTED_EDGE ( 'NONE', *, *, #17773, .F. ) ;
#54969=B_SPLINE_CURVE_WITH_KNOTS ( 'NONE', 3,
 ( #1177, #26888, #19264, #11652 ),
 .UNSPECIFIED., .F., .F.,
 ( 4, 4 ),
 ( 0.000000000000000000, 9.999999999998900014E-05 ),
 .UNSPECIFIED. ) ;
#54970=ORIENTED_EDGE ( 'NONE', *, *, #70450, .T. ) ;
#54971=DIRECTION ( 'NONE',  ( 3.773278334444166432E-23, -1.000000000000000000, 0.000000000000000000 ) ) ;
#54972=CARTESIAN_POINT ( 'NONE',  ( -31.24388727629348139, -25.16930718282847579, 7.183628892452282422 ) ) ;
#54973=CARTESIAN_POINT ( 'NONE',  ( 13.55612473118199723, -16.30799122071102403, -1.500000000000002220 ) ) ;
#54974=CARTESIAN_POINT ( 'NONE',  ( -94.62287095715001328, -24.51283580621365132, 0.6167428607019771469 ) ) ;
#54975=PLANE ( 'NONE',  #53492 ) ;
#54978=CARTESIAN_POINT ( 'NONE',  ( 11.07193147992585835, -15.93265361536492364, 11.49999999999998934 ) ) ;
#54979=CARTESIAN_POINT ( 'NONE',  ( -51.92621816357582532, -25.27152954406082230, 6.039110851711205541 ) ) ;
#54980=EDGE_LOOP ( 'NONE', ( #29361, #72765, #25030, #21570 ) ) ;
#54981=CARTESIAN_POINT ( 'NONE',  ( 12.63578256557813795, 14.83599306707809085, 11.49999999999999645 ) ) ;
#54983=AXIS2_PLACEMENT_3D ( 'NONE', #35812, #90099, #20573 ) ;
#54985=ADVANCED_FACE ( 'NONE', ( #40646 ), #24902, .F. ) ;
#54986=ORIENTED_EDGE ( 'NONE', *, *, #91014, .T. ) ;
#54987=CARTESIAN_POINT ( 'NONE',  ( -58.62287095715004881, -24.50321055353806443, 9.387540953477540029 ) ) ;
#54988=CARTESIAN_POINT ( 'NONE',  ( -70.35227678678285201, -25.30467589278440244, 4.853662785711239991 ) ) ;
#54991=EDGE_CURVE ( 'NONE', #37559, #15956, #62994, .T. ) ;
#54992=CARTESIAN_POINT ( 'NONE',  ( -55.62287095715009144, -24.15431212366392444, -0.2830839119429288120 ) ) ;
#54993=CARTESIAN_POINT ( 'NONE',  ( -14.15603575923578283, -13.64839490926926580, 11.49999999999998934 ) ) ;
#54995=CARTESIAN_POINT ( 'NONE',  ( -41.29362909362059497, -25.31583684833336179, 4.684754115636811989 ) ) ;
#54997=CARTESIAN_POINT ( 'NONE',  ( -15.49073194614445015, 15.02706685249526686, -1.500000000000002220 ) ) ;
#55001=CARTESIAN_POINT ( 'NONE',  ( -46.52287095715007581, -23.47593901973090524, -1.443836447538997314 ) ) ;
#55003=VECTOR ( 'NONE', #82284, 1000.000000000000114 ) ;
#55006=DIRECTION ( 'NONE',  ( 0.000000000000000000, 0.9999999999976377785, 2.173523156925979128E-06 ) ) ;
#55007=DIRECTION ( 'NONE',  ( 0.000000000000000000, 0.9999999999976377785, 2.173523156925979975E-06 ) ) ;
#55009=PLANE ( 'NONE',  #20744 ) ;
#55010=CARTESIAN_POINT ( 'NONE',  ( -110.0268685312161665, -25.19071142001657293, 3.335046394459539876 ) ) ;
#55011=CARTESIAN_POINT ( 'NONE',  ( -98.52287095715006160, -24.64898659630368272, 1.056161002820829697 ) ) ;
#55012=CARTESIAN_POINT ( 'NONE',  ( -111.3776484685884327, -25.29779381075475442, 4.332404409858182426 ) ) ;
#55013=CARTESIAN_POINT ( 'NONE',  ( -3.169371320753151977, 19.67850563098683736, 11.49999999999998934 ) ) ;
#55014=CARTESIAN_POINT ( 'NONE',  ( -41.62287095715006302, -23.48783264082477729, -1.443836473390071928 ) ) ;
#55015=CARTESIAN_POINT ( 'NONE',  ( -11.18921147948170614, -16.41150865552512883, -1.500000000000002220 ) ) ;
#55017=CARTESIAN_POINT ( 'NONE',  ( -33.62287095715005592, -24.64898659630367206, 1.056161002820817485 ) ) ;
#55018=LINE ( 'NONE', #40784, #73441 ) ;
#55019=CARTESIAN_POINT ( 'NONE',  ( -10.32638548400381673, 17.97674989526738898, 11.49999999999999645 ) ) ;
#55022=DIRECTION ( 'NONE',  ( 0.000000000000000000, -0.9999999999976377785, -2.173523156925979128E-06 ) ) ;
#55023=CARTESIAN_POINT ( 'NONE',  ( 21.14626179850551324, 8.528272852130310611, 11.49999999999999645 ) ) ;
#55024=ORIENTED_EDGE ( 'NONE', *, *, #93759, .F. ) ;
#55025=CARTESIAN_POINT ( 'NONE',  ( -83.62287095715012697, -24.35013146730204170, 9.818937971375106599 ) ) ;
#55027=ORIENTED_EDGE ( 'NONE', *, *, #20421, .F. ) ;
#55028=CARTESIAN_POINT ( 'NONE',  ( 18.20877288740043198, -8.745817889818592761, 11.49999999999998934 ) ) ;
#55030=CARTESIAN_POINT ( 'NONE',  ( -69.62287095715005592, -23.48783264082478084, -1.443836473390067265 ) ) ;
#55031=ORIENTED_EDGE ( 'NONE', *, *, #38030, .T. ) ;
#55032=B_SPLINE_CURVE_WITH_KNOTS ( 'NONE', 3,
 ( #27650, #26648, #41883, #58594, #72831, #3330 ),
 .UNSPECIFIED., .F., .F.,
 ( 4, 2, 4 ),
 ( 6.384118694792690538E-06, 0.001386860460836467687, 0.002767336802978142760 ),
 .UNSPECIFIED. ) ;
#55033=B_SPLINE_CURVE_WITH_KNOTS ( 'NONE', 3,
 ( #79709, #13062, #11206, #74958 ),
 .UNSPECIFIED., .F., .F.,
 ( 4, 4 ),
 ( 0.000000000000000000, 1.000000000000000000 ),
 .UNSPECIFIED. ) ;
#55036=CARTESIAN_POINT ( 'NONE',  ( -21.13427563780003382, 8.902639844219676135, 11.49999999999998934 ) ) ;
#55037=CARTESIAN_POINT ( 'NONE',  ( -51.26181408848110976, -25.27420670906736078, 3.790032851153764870 ) ) ;
#55038=CARTESIAN_POINT ( 'NONE',  ( -17.57154585214776077, 12.61476001598989782, -1.500000000000002220 ) ) ;
#55039=CARTESIAN_POINT ( 'NONE',  ( -104.6228709571500559, -24.65952944569304961, 1.056160979905701236 ) ) ;
#55040=CARTESIAN_POINT ( 'NONE',  ( -13.85205798638896901, 15.75786377350088507, 11.49999999999999645 ) ) ;
#55042=CARTESIAN_POINT ( 'NONE',  ( -52.62287095715005592, -29.50247984919015209, -1.443849546365058689 ) ) ;
#55043=CARTESIAN_POINT ( 'NONE',  ( -124.5198396697245045, -24.51314013834317151, 0.6176544820404232805 ) ) ;
#55044=CARTESIAN_POINT ( 'NONE',  ( -1.213202359833694732, 22.00568734548514627, 11.49999999999998934 ) ) ;
#55048=CARTESIAN_POINT ( 'NONE',  ( -49.79812375574695693, -25.27344795505599961, 3.459241572631841954 ) ) ;
#55049=CARTESIAN_POINT ( 'NONE',  ( -106.6228709571500559, -23.47596703998600631, 11.44779298504227860 ) ) ;
#55051=PLANE ( 'NONE',  #66469 ) ;
#55054=ORIENTED_EDGE ( 'NONE', *, *, #51860, .T. ) ;
#55059=CARTESIAN_POINT ( 'NONE',  ( -7.302954156136775232, -19.11528491071161540, -1.500000000000002220 ) ) ;
#55064=CARTESIAN_POINT ( 'NONE',  ( -14.60993195340527251, 16.82711592829100411, 11.49999999999998934 ) ) ;
#55065=CARTESIAN_POINT ( 'NONE',  ( -101.6228709571500559, -24.64965695001469115, 8.947790433994178727 ) ) ;
#55066=CARTESIAN_POINT ( 'NONE',  ( -27.61134344903479843, -24.63328469850957347, 8.250456965916750818 ) ) ;
#55073=CARTESIAN_POINT ( 'NONE',  ( 0.5783248939474509021, 20.82821387695577187, -1.500000000000002220 ) ) ;
#55074=EDGE_CURVE ( 'NONE', #23903, #40713, #49737, .T. ) ;
#55075=ORIENTED_EDGE ( 'NONE', *, *, #95265, .T. ) ;
#55076=CARTESIAN_POINT ( 'NONE',  ( -51.52287095715006870, -24.64898659630367206, 1.056161002820821038 ) ) ;
#55077=ORIENTED_EDGE ( 'NONE', *, *, #29999, .T. ) ;
#55078=VERTEX_POINT ( 'NONE', #27908 ) ;
#55080=CARTESIAN_POINT ( 'NONE',  ( -51.49483116284216067, -25.12217715923064176, 6.426654410346007040 ) ) ;
#55081=CARTESIAN_POINT ( 'NONE',  ( -7.324709186033012465, -19.69651249574825513, -1.500000000000002220 ) ) ;
#55082=ORIENTED_EDGE ( 'NONE', *, *, #87437, .T. ) ;
#55084=CARTESIAN_POINT ( 'NONE',  ( -53.52287095715009002, -23.72773821059537269, 11.05748984161097503 ) ) ;
#55087=CARTESIAN_POINT ( 'NONE',  ( -119.5228709571500758, -23.48786465467241769, 11.44779295918253759 ) ) ;
#55088=CARTESIAN_POINT ( 'NONE',  ( -64.52287095715004739, -24.50321055353805377, 9.387540953477524042 ) ) ;
#55089=CARTESIAN_POINT ( 'NONE',  ( 7.537409830304743430, 20.87355781386819942, 11.49999999999999645 ) ) ;
#55090=VERTEX_POINT ( 'NONE', #3094 ) ;
#55091=EDGE_CURVE ( 'NONE', #64522, #73782, #55741, .T. ) ;
#55092=PLANE ( 'NONE',  #32388 ) ;
#55093=CARTESIAN_POINT ( 'NONE',  ( -38.62287095715005592, -23.96127896941631619, -0.6493128931037943641 ) ) ;
#55094=ORIENTED_EDGE ( 'NONE', *, *, #59641, .T. ) ;
#55095=CARTESIAN_POINT ( 'NONE',  ( -21.16080155796574047, 8.166215375980355518, -1.500000000000002220 ) ) ;
#55097=ORIENTED_EDGE ( 'NONE', *, *, #10027, .F. ) ;
#55100=CARTESIAN_POINT ( 'NONE',  ( -3.510519812331947875, -19.85243952969433323, -1.500000000000002220 ) ) ;
#55103=DIRECTION ( 'NONE',  ( -3.773278334444167608E-23, 1.000000000000000000, 0.000000000000000000 ) ) ;
#55104=CARTESIAN_POINT ( 'NONE',  ( -8.193370562272118462, -20.86776251599019361, -1.500000000000002220 ) ) ;
#55105=ADVANCED_FACE ( 'NONE', ( #95424 ), #65251, .T. ) ;
#55107=ORIENTED_EDGE ( 'NONE', *, *, #9452, .T. ) ;
#55108=CARTESIAN_POINT ( 'NONE',  ( -101.1944152955115044, -25.16257438707235039, 6.858246049920544429 ) ) ;
#55109=CARTESIAN_POINT ( 'NONE',  ( -48.62287095715004881, -24.66019654487199020, 8.947790411086135265 ) ) ;
#55110=CARTESIAN_POINT ( 'NONE',  ( -96.58953762381672448, -23.47596703998600631, 11.44779298504227683 ) ) ;
#55111=DIRECTION ( 'NONE',  ( 3.773278334444168195E-23, -1.000000000000000000, 0.000000000000000000 ) ) ;
#55112=LINE ( 'NONE', #62230, #16338 ) ;
#55114=CARTESIAN_POINT ( 'NONE',  ( -14.26233628608129855, 13.40890954296891024, -1.500000000000002220 ) ) ;
#55116=ORIENTED_EDGE ( 'NONE', *, *, #3857, .F. ) ;
#55117=CARTESIAN_POINT ( 'NONE',  ( 16.48747857468482891, 13.79107804547330929, -1.500000000000002220 ) ) ;
#55118=CARTESIAN_POINT ( 'NONE',  ( -36.52287095715006870, -24.65952944569304606, 1.056160979905691910 ) ) ;
#55120=CARTESIAN_POINT ( 'NONE',  ( -59.52287095715006160, -23.48783264082477018, -1.443836473390095021 ) ) ;
#55121=AXIS2_PLACEMENT_3D ( 'NONE', #58066, #5251, #50437 ) ;
#55122=CARTESIAN_POINT ( 'NONE',  ( -92.62287095715005592, -29.50248528299804818, 1.056150453629040253 ) ) ;
#55123=CARTESIAN_POINT ( 'NONE',  ( -19.55383134093860420, 11.88776249338449986, -1.500000000000002220 ) ) ;
#55125=EDGE_CURVE ( 'NONE', #3631, #36107, #31446, .T. ) ;
#55127=B_SPLINE_CURVE_WITH_KNOTS ( 'NONE', 3,
 ( #97753, #29237, #14003, #90147 ),
 .UNSPECIFIED., .F., .F.,
 ( 4, 4 ),
 ( 0.000000000000000000, 0.0001000000000000028644 ),
 .UNSPECIFIED. ) ;
#55130=CARTESIAN_POINT ( 'NONE',  ( 7.608091486120485136, 18.53616061196756704, 11.49999999999999645 ) ) ;
#55131=CARTESIAN_POINT ( 'NONE',  ( -79.92757955003747838, -25.26612385862897980, 4.561565571244288186 ) ) ;
#55132=CARTESIAN_POINT ( 'NONE',  ( -107.5562042904834072, -24.64898659630528854, 1.056161002820829919 ) ) ;
#55137=CARTESIAN_POINT ( 'NONE',  ( -85.62287095715009855, -24.14321612903114911, -0.2833117244521602407 ) ) ;
#55139=CARTESIAN_POINT ( 'NONE',  ( -20.93004649427559016, -6.003493321846349318, -1.500000000000002220 ) ) ;
#55141=CARTESIAN_POINT ( 'NONE',  ( -18.24527198174902765, 7.358211898524878336, -1.500000000000002220 ) ) ;
#55142=CARTESIAN_POINT ( 'NONE',  ( -85.52287095715011844, -24.52323809116985132, 9.355190652339427260 ) ) ;
#55143=B_SPLINE_CURVE_WITH_KNOTS ( 'NONE', 3,
 ( #5884, #29224, #52568, #83501, #13986, #44963, #75888, #84003, #94615, #24097, #55571, #64196, #31720, #62183, #1775, #70288, #93602, #8883, #55066, #39325 ),
 .UNSPECIFIED., .F., .F.,
 ( 4, 2, 2, 2, 2, 2, 2, 2, 2, 4 ),
 ( 8.673617379884034509E-19, 0.0005507670852896362143, 0.001101534170579271561, 0.001652301255868906908, 0.002203068341158542255, 0.002753835426448177602, 0.003304602511737812949, 0.003855369597027447862, 0.004130753139672266837, 0.004406136682317085378 ),
 .UNSPECIFIED. ) ;
#55148=CARTESIAN_POINT ( 'NONE',  ( -56.62287095715005592, -24.50321055353805022, 9.387540953477531147 ) ) ;
#55149=CARTESIAN_POINT ( 'NONE',  ( -73.62287095715007013, -23.73934037231756733, 11.05740245334329153 ) ) ;
#55150=CARTESIAN_POINT ( 'NONE',  ( -9.016818060619870678, -18.48156098877705844, 11.49999999999999645 ) ) ;
#55153=EDGE_CURVE ( 'NONE', #85265, #80623, #42160, .T. ) ;
#55155=CARTESIAN_POINT ( 'NONE',  ( 11.26306171725914851, -19.60737681494043727, 11.49999999999999645 ) ) ;
#55156=ORIENTED_EDGE ( 'NONE', *, *, #10026, .F. ) ;
#55158=CARTESIAN_POINT ( 'NONE',  ( -70.03562343076868046, -25.25639593825284024, 7.066378759041874957 ) ) ;
#55160=CARTESIAN_POINT ( 'NONE',  ( -125.6244067124949169, -24.52399227489127043, 9.353111116836528183 ) ) ;
#55162=EDGE_CURVE ( 'NONE', #98033, #69591, #14551, .T. ) ;
#55166=EDGE_CURVE ( 'NONE', #71187, #70309, #61369, .T. ) ;
#55168=CARTESIAN_POINT ( 'NONE',  ( -79.71799800425125682, -25.26749921723603975, 5.176233770711395898 ) ) ;
#55169=CARTESIAN_POINT ( 'NONE',  ( 13.81544771398824345, -18.15223324129861382, -1.500000000000002220 ) ) ;
#55170=FACE_OUTER_BOUND ( 'NONE', #29220, .T. ) ;
#55171=CARTESIAN_POINT ( 'NONE',  ( -115.5228709571500616, -23.47596703998600631, 11.44779298504227860 ) ) ;
#55172=PLANE ( 'NONE',  #17677 ) ;
#55173=CARTESIAN_POINT ( 'NONE',  ( 22.44084908143146251, -0.7541981612834567361, 11.49999999999999645 ) ) ;
#55175=CARTESIAN_POINT ( 'NONE',  ( -70.62287095715008434, -24.15516710230295416, 10.28746687063725318 ) ) ;
#55176=CARTESIAN_POINT ( 'NONE',  ( 9.922928194174257754, 19.57116106031148561, -1.500000000000002220 ) ) ;
#55177=CARTESIAN_POINT ( 'NONE',  ( -113.5228709571500758, -24.51283580621365488, 0.6167428607019769249 ) ) ;
#55178=B_SPLINE_CURVE_WITH_KNOTS ( 'NONE', 3,
 ( #45573, #98836, #60303, #91227, #21704, #52676, #83613, #14098 ),
 .UNSPECIFIED., .F., .F.,
 ( 4, 2, 2, 4 ),
 ( 6.384118696468709548E-06, 0.002007151183516189211, 0.003007534715926047687, 0.004007918248335905730 ),
 .UNSPECIFIED. ) ;
#55179=CARTESIAN_POINT ( 'NONE',  ( -44.63403588481693163, -24.35071581493542681, 9.817618358456025263 ) ) ;
#55180=CARTESIAN_POINT ( 'NONE',  ( -56.55620429048340725, -23.48786465467241058, 11.44779295918254824 ) ) ;
#55181=ORIENTED_EDGE ( 'NONE', *, *, #80707, .T. ) ;
#55185=CARTESIAN_POINT ( 'NONE',  ( -18.82070947631147106, 8.064391923812276985, 11.49999999999998934 ) ) ;
#55188=VERTEX_POINT ( 'NONE', #5067 ) ;
#55191=CARTESIAN_POINT ( 'NONE',  ( 1.912052097559287844, -22.98750448113701239, -1.500000000000002220 ) ) ;
#55192=CARTESIAN_POINT ( 'NONE',  ( -49.61653484136814996, -25.15870442618641789, 3.051990030215718797 ) ) ;
#55193=CARTESIAN_POINT ( 'NONE',  ( -11.05657426389776354, 17.00066307926000420, -1.500000000000002220 ) ) ;
#55197=CARTESIAN_POINT ( 'NONE',  ( -44.62287095715004881, -24.66019654487198665, 8.947790411086135265 ) ) ;
#55199=CARTESIAN_POINT ( 'NONE',  ( -14.42888051209446409, 15.91495273949476363, 11.49999999999999645 ) ) ;
#55201=CARTESIAN_POINT ( 'NONE',  ( -75.61136025641945935, -23.48783264082477018, -1.443836473390089914 ) ) ;
#55203=ORIENTED_EDGE ( 'NONE', *, *, #1924, .F. ) ;
#55204=CARTESIAN_POINT ( 'NONE',  ( -5.954758479537505700, 19.85987847461844424, -1.500000000000002220 ) ) ;
#55205=AXIS2_PLACEMENT_3D ( 'NONE', #16992, #39332, #47457 ) ;
#55206=EDGE_CURVE ( 'NONE', #61568, #84539, #32703, .T. ) ;
#55208=CARTESIAN_POINT ( 'NONE',  ( -125.6257035845457750, -23.85016227208582151, -0.8807180028928047744 ) ) ;
#55209=ORIENTED_EDGE ( 'NONE', *, *, #63936, .F. ) ;
#55210=EDGE_CURVE ( 'NONE', #22015, #38564, #22768, .T. ) ;
#55211=CARTESIAN_POINT ( 'NONE',  ( -111.5879331448754641, -24.51419770103157703, 9.386484678747162747 ) ) ;
#55212=CARTESIAN_POINT ( 'NONE',  ( -129.5562042904834072, -23.47596703998600631, 11.44779298504227683 ) ) ;
#55213=VERTEX_POINT ( 'NONE', #67982 ) ;
#55214=ORIENTED_EDGE ( 'NONE', *, *, #33867, .T. ) ;
#55216=CARTESIAN_POINT ( 'NONE',  ( -42.66381526571083072, -23.48786465467240347, 11.44779295918255535 ) ) ;
#55218=CARTESIAN_POINT ( 'NONE',  ( -20.87105610827876134, -7.033761084331515256, 11.49999999999999645 ) ) ;
#55220=CARTESIAN_POINT ( 'NONE',  ( -89.63160444167392882, -24.15620529776628445, 10.23563542870660115 ) ) ;
#55221=CARTESIAN_POINT ( 'NONE',  ( -12.77507031947300042, 18.62636059118606724, -1.500000000000002220 ) ) ;
#55222=CARTESIAN_POINT ( 'NONE',  ( -10.24336464640716216, -18.35016636821181280, 11.49999999999998934 ) ) ;
#55223=ADVANCED_FACE ( 'NONE', ( #29900 ), #6064, .F. ) ;
#55230=DIRECTION ( 'NONE',  ( 3.773278334444166432E-23, -1.000000000000000000, 0.000000000000000000 ) ) ;
#55233=VERTEX_POINT ( 'NONE', #91302 ) ;
#55234=CARTESIAN_POINT ( 'NONE',  ( 4.565063516603933280, 20.63981631578574039, -1.500000000000002220 ) ) ;
#55236=CARTESIAN_POINT ( 'NONE',  ( -58.86390871394272040, -25.03722704563418944, 7.590184509431679771 ) ) ;
#55238=CARTESIAN_POINT ( 'NONE',  ( -118.5562042904833930, -23.47593901973091235, -1.443836447538997536 ) ) ;
#55240=CARTESIAN_POINT ( 'NONE',  ( -0.9571703918902072505, -22.19477237104690914, -1.500000000000002220 ) ) ;
#55241=CARTESIAN_POINT ( 'NONE',  ( -81.59989503929168109, -23.73791477778912196, 11.05961554403170943 ) ) ;
#55244=CARTESIAN_POINT ( 'NONE',  ( -37.56099248051968686, -23.73766607897670866, -1.055555164236442245 ) ) ;
#55245=CARTESIAN_POINT ( 'NONE',  ( -126.5909412814345814, -23.48783264082477018, -1.443836473390087027 ) ) ;
#55247=CARTESIAN_POINT ( 'NONE',  ( -67.52287095715006160, -29.50250786944525672, 11.44777988621623699 ) ) ;
#55248=CARTESIAN_POINT ( 'NONE',  ( -17.65537929698502495, 8.214918384300796461, -1.500000000000002220 ) ) ;
#55249=CARTESIAN_POINT ( 'NONE',  ( 4.431377227695222132, -20.94745169971119481, -1.500000000000002220 ) ) ;
#55250=PLANE ( 'NONE',  #14205 ) ;
#55251=CARTESIAN_POINT ( 'NONE',  ( -60.57813319489011405, -24.92592662360294042, 8.075495902990192931 ) ) ;
#55252=FACE_OUTER_BOUND ( 'NONE', #73183, .T. ) ;
#55253=CARTESIAN_POINT ( 'NONE',  ( -124.6228709571500559, -29.50250243563736774, 8.947779886222134493 ) ) ;
#55254=CARTESIAN_POINT ( 'NONE',  ( 20.21490908150494192, 10.32750977814155391, -1.500000000000002220 ) ) ;
#55257=CARTESIAN_POINT ( 'NONE',  ( -1.769646468872753120, 19.80360307839763934, 11.49999999999999645 ) ) ;
#55258=CARTESIAN_POINT ( 'NONE',  ( -123.6238837146930933, -24.51419770103158768, 9.386484678747160970 ) ) ;
#55259=DIRECTION ( 'NONE',  ( 0.000000000000000000, 0.9999999999976377785, 2.173523156925979975E-06 ) ) ;
#55260=CARTESIAN_POINT ( 'NONE',  ( -41.62287095715006302, -23.47596703998600276, 11.44779298504227505 ) ) ;
#55263=DIRECTION ( 'NONE',  ( 0.000000000000000000, 0.9999999999976377785, 2.173523156925979128E-06 ) ) ;
#55264=CARTESIAN_POINT ( 'NONE',  ( -51.70072539166533687, -25.27412478701024412, 3.987152057456385901 ) ) ;
#55265=CARTESIAN_POINT ( 'NONE',  ( -21.63489631200954122, -1.325961216813365429, 11.49999999999998934 ) ) ;
#55266=CARTESIAN_POINT ( 'NONE',  ( -56.58273429346868255, -24.51419770103157347, 9.386484678747180510 ) ) ;
#55267=CARTESIAN_POINT ( 'NONE',  ( -7.007757480239389380, 18.17491015770016816, -1.500000000000002220 ) ) ;
#55268=CARTESIAN_POINT ( 'NONE',  ( -61.62287095715005592, -24.33927499327855415, 9.819080762295822495 ) ) ;
#55270=CARTESIAN_POINT ( 'NONE',  ( 20.35419724272142616, 1.316291261081859787, 11.49999999999999645 ) ) ;
#55271=DIRECTION ( 'NONE',  ( -3.773278334453079618E-23, 0.9999999999976377785, 2.173523156925979975E-06 ) ) ;
#55274=EDGE_CURVE ( 'NONE', #67048, #29423, #76558, .T. ) ;
#55275=ORIENTED_EDGE ( 'NONE', *, *, #45606, .T. ) ;
#55276=CARTESIAN_POINT ( 'NONE',  ( -41.46433198031985512, -25.28409534238342715, 4.125402634550018099 ) ) ;
#55278=CARTESIAN_POINT ( 'NONE',  ( -48.87629837916329478, -25.31602057134209360, 6.044965623264298316 ) ) ;
#55280=B_SPLINE_CURVE_WITH_KNOTS ( 'NONE', 3,
 ( #5727, #3752, #36188, #82352 ),
 .UNSPECIFIED., .F., .F.,
 ( 4, 4 ),
 ( 0.000000000000000000, 9.999999999998897304E-05 ),
 .UNSPECIFIED. ) ;
#55282=CARTESIAN_POINT ( 'NONE',  ( 6.297820759360134524, 19.07352124001985771, 11.49999999999998934 ) ) ;
#55283=CARTESIAN_POINT ( 'NONE',  ( -57.62287095715004881, -23.47593901973091235, -1.443836447539007972 ) ) ;
#55284=ORIENTED_EDGE ( 'NONE', *, *, #73738, .T. ) ;
#55285=ADVANCED_FACE ( 'NONE', ( #53253 ), #97903, .F. ) ;
#55288=EDGE_CURVE ( 'NONE', #84515, #16871, #27859, .T. ) ;
#55289=AXIS2_PLACEMENT_3D ( 'NONE', #24530, #698, #53512 ) ;
#55290=CARTESIAN_POINT ( 'NONE',  ( 7.457602374657920308, -21.66695214233757838, 11.49999999999999645 ) ) ;
#55291=CARTESIAN_POINT ( 'NONE',  ( 11.07647423179810531, -19.82844882884714366, 11.49999999999998934 ) ) ;
#55292=ORIENTED_EDGE ( 'NONE', *, *, #24002, .F. ) ;
#55293=CARTESIAN_POINT ( 'NONE',  ( -30.47287095715008931, -25.29768654522517224, 5.277398094566895459 ) ) ;
#55295=CARTESIAN_POINT ( 'NONE',  ( -46.62287095715004881, -24.65952944569304250, 1.056160979905693020 ) ) ;
#55296=EDGE_CURVE ( 'NONE', #12270, #97111, #54459, .T. ) ;
#55297=CARTESIAN_POINT ( 'NONE',  ( -30.57287095715006942, -24.39443487893185747, 0.3225640792553110536 ) ) ;
#55298=CARTESIAN_POINT ( 'NONE',  ( -128.5562989009644639, -23.48786465467242124, 11.44779295918253403 ) ) ;
#55299=CARTESIAN_POINT ( 'NONE',  ( -48.87557505443476202, -25.26869748743544264, 6.071662630268244598 ) ) ;
#55300=CARTESIAN_POINT ( 'NONE',  ( -98.89580656140421411, -25.31200720546054583, 6.002154695688947328 ) ) ;
#55302=CARTESIAN_POINT ( 'NONE',  ( 19.80222353126469415, -4.898785079568316547, 11.49999999999998934 ) ) ;
#55303=ORIENTED_EDGE ( 'NONE', *, *, #68054, .F. ) ;
#55304=EDGE_CURVE ( 'NONE', #61812, #82610, #47277, .T. ) ;
#55305=CARTESIAN_POINT ( 'NONE',  ( -22.04953120734539240, -6.464106996104416858, 11.49999999999998934 ) ) ;
#55308=CARTESIAN_POINT ( 'NONE',  ( -108.5923757939725078, -23.96169478059714208, 10.65365249895716993 ) ) ;
#55310=CARTESIAN_POINT ( 'NONE',  ( -53.58734467797736301, -24.35071581493542681, 9.817618358456032368 ) ) ;
#55311=CARTESIAN_POINT ( 'NONE',  ( -8.160016139516647726, -19.69179572373923648, 11.49999999999999645 ) ) ;
#55312=ORIENTED_EDGE ( 'NONE', *, *, #74359, .F. ) ;
#55313=VERTEX_POINT ( 'NONE', #47642 ) ;
#55314=CARTESIAN_POINT ( 'NONE',  ( -2.380169663812839342, 22.11153957539610104, -1.500000000000002220 ) ) ;
#55315=B_SPLINE_CURVE_WITH_KNOTS ( 'NONE', 3,
 ( #36201, #28090, #12844, #35704 ),
 .UNSPECIFIED., .F., .F.,
 ( 4, 4 ),
 ( 0.000000000000000000, 1.000000000000000000 ),
 .UNSPECIFIED. ) ;
#55316=CARTESIAN_POINT ( 'NONE',  ( -12.00526669028610272, -16.82065764665920682, -1.500000000000002220 ) ) ;
#55317=EDGE_CURVE ( 'NONE', #73668, #81696, #93191, .T. ) ;
#55318=ORIENTED_EDGE ( 'NONE', *, *, #49118, .F. ) ;
#55319=CARTESIAN_POINT ( 'NONE',  ( -112.6228709571500559, -23.47596703998600631, 11.44779298504227860 ) ) ;
#55320=CARTESIAN_POINT ( 'NONE',  ( -70.79082562273967483, -25.25978459231412288, 3.590539514744167437 ) ) ;
#55321=VERTEX_POINT ( 'NONE', #46642 ) ;
#55324=CARTESIAN_POINT ( 'NONE',  ( -49.62287095715005592, -23.48783264082478084, -1.443836473390070596 ) ) ;
#55326=CARTESIAN_POINT ( 'NONE',  ( -20.80165436122882383, -1.723964017131293103, -1.500000000000002220 ) ) ;
#55327=CARTESIAN_POINT ( 'NONE',  ( 21.83365961380331655, 0.8745889840297637052, 11.49999999999999645 ) ) ;
#55328=EDGE_CURVE ( 'NONE', #82055, #64861, #1191, .T. ) ;
#55329=CARTESIAN_POINT ( 'NONE',  ( -85.62287095715005592, -23.47596703998600631, 11.44779298504227860 ) ) ;
#55331=CARTESIAN_POINT ( 'NONE',  ( 19.74966320730700176, -10.79507447929251107, 11.49999999999998934 ) ) ;
#55332=B_SPLINE_CURVE_WITH_KNOTS ( 'NONE', 3,
 ( #23833, #54805, #85744, #14214 ),
 .UNSPECIFIED., .F., .F.,
 ( 4, 4 ),
 ( 1.387778780781445521E-17, 9.999999999997510880E-05 ),
 .UNSPECIFIED. ) ;
#55333=EDGE_CURVE ( 'NONE', #12687, #3446, #52054, .T. ) ;
#55335=CARTESIAN_POINT ( 'NONE',  ( -122.5228709571500758, -23.47593901973090524, -1.443836447538996204 ) ) ;
#55336=CARTESIAN_POINT ( 'NONE',  ( -78.55620429048340725, -23.48783264082478084, -1.443836473390064157 ) ) ;
#55337=VERTEX_POINT ( 'NONE', #40018 ) ;
#55338=ORIENTED_EDGE ( 'NONE', *, *, #92120, .F. ) ;
#55340=AXIS2_PLACEMENT_3D ( 'NONE', #27679, #42425, #10442 ) ;
#55341=ORIENTED_EDGE ( 'NONE', *, *, #47565, .T. ) ;
#55342=CARTESIAN_POINT ( 'NONE',  ( -20.52298544035203776, 6.160189734329080125, -1.500000000000002220 ) ) ;
#55343=CARTESIAN_POINT ( 'NONE',  ( 16.92800457317958518, -14.60656088873787262, 11.49999999999999645 ) ) ;
#55345=CARTESIAN_POINT ( 'NONE',  ( 8.294003578737715543, -19.35633765900385939, -1.500000000000002220 ) ) ;
#55346=CARTESIAN_POINT ( 'NONE',  ( -30.54276571906597226, -24.67129498985978131, 8.908675929220796874 ) ) ;
#55347=CARTESIAN_POINT ( 'NONE',  ( 19.20567810191101898, 5.375360269454119155, -1.500000000000002220 ) ) ;
#55348=CARTESIAN_POINT ( 'NONE',  ( -117.6228709571499706, -24.51283580621365132, 0.6167428607019862508 ) ) ;
#55349=CARTESIAN_POINT ( 'NONE',  ( -43.52287095715006870, -23.73934037231756022, 11.05740245334330041 ) ) ;
#55350=CARTESIAN_POINT ( 'NONE',  ( 7.855769811932122870, -20.56199346058834720, -1.500000000000002220 ) ) ;
#55353=DIRECTION ( 'NONE',  ( -3.773278334453079030E-23, 0.9999999999976377785, 2.173523156925979128E-06 ) ) ;
#55354=CARTESIAN_POINT ( 'NONE',  ( -70.62287095715005592, -23.47593901973091235, -1.443836447539006196 ) ) ;
#55355=CARTESIAN_POINT ( 'NONE',  ( 5.313885144808909722, 20.14914662543312929, 11.49999999999999645 ) ) ;
#55358=CARTESIAN_POINT ( 'NONE',  ( -108.6228709571500843, -23.96177878511308990, 10.65340807706329684 ) ) ;
#55361=CARTESIAN_POINT ( 'NONE',  ( -20.61954105445765251, -5.431428859615135885, -1.500000000000002220 ) ) ;
#55362=DIRECTION ( 'NONE',  ( 1.000000000000000000, 3.773278334444166432E-23, 8.201307841325785021E-29 ) ) ;
#55363=CARTESIAN_POINT ( 'NONE',  ( -51.29013145356853443, -25.26457908625394566, 3.888394836251752196 ) ) ;
#55364=FACE_OUTER_BOUND ( 'NONE', #22986, .T. ) ;
#55366=CARTESIAN_POINT ( 'NONE',  ( 21.68943130245101258, -6.005725296444199834, -1.500000000000002220 ) ) ;
#55370=CARTESIAN_POINT ( 'NONE',  ( -31.53769362740780480, -24.35071581493542325, 9.817618358456039473 ) ) ;
#55371=CARTESIAN_POINT ( 'NONE',  ( -11.91260469445801995, 15.66180005371307260, 11.49999999999999645 ) ) ;
#55372=CARTESIAN_POINT ( 'NONE',  ( -49.52287095715006160, -24.64898659630367561, 1.056161002820821038 ) ) ;
#55373=CARTESIAN_POINT ( 'NONE',  ( -30.57287095715006231, -29.50248298729120222, -6.412432995908637812E-05 ) ) ;
#55375=CARTESIAN_POINT ( 'NONE',  ( -99.55027089583788324, -24.34968618360934300, 0.1864209137778966852 ) ) ;
#55376=CARTESIAN_POINT ( 'NONE',  ( -55.62287095715004170, -24.91544648472619983, 1.928969306349233470 ) ) ;
#55377=FACE_OUTER_BOUND ( 'NONE', #21977, .T. ) ;
#55379=CARTESIAN_POINT ( 'NONE',  ( -0.9724026449420489771, -19.73431249065222204, 11.49999999999998934 ) ) ;
#55380=VERTEX_POINT ( 'NONE', #54757 ) ;
#55381=CARTESIAN_POINT ( 'NONE',  ( 17.97931717627152182, 9.192180251422895410, 11.49999999999999645 ) ) ;
#55385=ORIENTED_EDGE ( 'NONE', *, *, #19224, .T. ) ;
#55386=CARTESIAN_POINT ( 'NONE',  ( -100.5228709571500616, -24.99156044556120904, 7.747789690856173195 ) ) ;
#55391=CARTESIAN_POINT ( 'NONE',  ( -67.62287095715005592, -24.64965695001468404, 8.947790433994184056 ) ) ;
#55392=ADVANCED_FACE ( 'NONE', ( #9565 ), #39519, .T. ) ;
#55394=CARTESIAN_POINT ( 'NONE',  ( 17.55240489776628721, -9.587225365216566431, -1.500000000000002220 ) ) ;
#55395=B_SPLINE_CURVE_WITH_KNOTS ( 'NONE', 3,
 ( #57275, #81588, #97307, #12058, #58745, #89696 ),
 .UNSPECIFIED., .F., .F.,
 ( 4, 2, 4 ),
 ( 0.000000000000000000, 0.001380901958385383774, 0.002761803916770767548 ),
 .UNSPECIFIED. ) ;
#55396=EDGE_CURVE ( 'NONE', #8604, #21913, #3718, .T. ) ;
#55398=CARTESIAN_POINT ( 'NONE',  ( -45.62317026584761237, -23.48786465467240703, 11.44779295918255002 ) ) ;
#55399=VERTEX_POINT ( 'NONE', #63884 ) ;
#55404=CARTESIAN_POINT ( 'NONE',  ( -100.5562042904833930, -23.48786465467241769, 11.44779295918254114 ) ) ;
#55405=B_SPLINE_CURVE_WITH_KNOTS ( 'NONE', 3,
 ( #361, #99799, #93705, #92698, #53667, #70379 ),
 .UNSPECIFIED., .F., .F.,
 ( 4, 2, 4 ),
 ( 0.000000000000000000, 0.001380901958385393315, 0.002761803916770786630 ),
 .UNSPECIFIED. ) ;
#55406=VECTOR ( 'NONE', #63515, 1000.000000000000114 ) ;
#55409=CARTESIAN_POINT ( 'NONE',  ( -106.6228709571500559, -23.47593901973091235, -1.443836447538999312 ) ) ;
#55410=CARTESIAN_POINT ( 'NONE',  ( -101.9683921942802982, -25.31392319263090229, 5.203681702801227438 ) ) ;
#55411=ORIENTED_EDGE ( 'NONE', *, *, #41584, .F. ) ;
#55412=CARTESIAN_POINT ( 'NONE',  ( 2.303441031721801480, -20.17751241584783628, 11.49999999999998934 ) ) ;
#55413=CARTESIAN_POINT ( 'NONE',  ( -39.56136241089613037, -29.50249502162446902, 5.536722193922502200 ) ) ;
#55415=ORIENTED_EDGE ( 'NONE', *, *, #30052, .T. ) ;
#55416=B_SPLINE_CURVE_WITH_KNOTS ( 'NONE', 3,
 ( #9444, #24658, #77439, #40403 ),
 .UNSPECIFIED., .F., .F.,
 ( 4, 4 ),
 ( 0.08881981938298308399, 0.08982056642374858235 ),
 .UNSPECIFIED. ) ;
#55417=CARTESIAN_POINT ( 'NONE',  ( -81.62287095715005592, -23.48783264082478794, -1.443836473390065711 ) ) ;
#55419=CARTESIAN_POINT ( 'NONE',  ( 15.40757771627215256, 13.04930689719894765, -1.500000000000002220 ) ) ;
#55420=CARTESIAN_POINT ( 'NONE',  ( 6.572693220633653688, -20.11273663914708365, 11.49999999999999645 ) ) ;
#55422=CARTESIAN_POINT ( 'NONE',  ( 18.07010470096111021, 12.80550835427630574, -1.500000000000002220 ) ) ;
#55423=CARTESIAN_POINT ( 'NONE',  ( 0.1292827521129817636, -20.55975067039486603, -1.500000000000002220 ) ) ;
#55424=CARTESIAN_POINT ( 'NONE',  ( -116.6228709571500559, -24.64898659630368627, 1.056161002820833028 ) ) ;
#55426=LINE ( 'NONE', #47808, #97682 ) ;
#55427=ORIENTED_EDGE ( 'NONE', *, *, #47154, .T. ) ;
#55429=CARTESIAN_POINT ( 'NONE',  ( -70.52287095715009002, -24.14406661686762945, 10.28769366194079282 ) ) ;
#55432=ORIENTED_EDGE ( 'NONE', *, *, #100352, .T. ) ;
#55434=DIRECTION ( 'NONE',  ( 0.000000000000000000, 0.9999999999976377785, 2.173523156925979975E-06 ) ) ;
#55436=CARTESIAN_POINT ( 'NONE',  ( -18.06733440434376092, 10.15830956056102963, -1.500000000000002220 ) ) ;
#55437=CARTESIAN_POINT ( 'NONE',  ( -15.83346750871019992, -14.79491179806518630, 11.49999999999999645 ) ) ;
#55438=EDGE_LOOP ( 'NONE', ( #41227, #88296, #98107, #76387 ) ) ;
#55439=CARTESIAN_POINT ( 'NONE',  ( -100.5895376238167387, -23.47596703998600631, 11.44779298504227683 ) ) ;
#55441=CARTESIAN_POINT ( 'NONE',  ( -18.60458529277170214, -12.42720982490441095, -1.500000000000002220 ) ) ;
#55442=EDGE_CURVE ( 'NONE', #3403, #63553, #37486, .T. ) ;
#55443=CARTESIAN_POINT ( 'NONE',  ( -47.48415699084505803, -24.66019654487199730, 8.947790411086117501 ) ) ;
#55444=CARTESIAN_POINT ( 'NONE',  ( -75.22287095715006444, -23.47596703998600631, 11.44779298504227860 ) ) ;
#55445=VERTEX_POINT ( 'NONE', #31404 ) ;
#55446=CARTESIAN_POINT ( 'NONE',  ( -118.7286108204959163, -25.33572373775064790, 6.311492575451646658 ) ) ;
#55447=CARTESIAN_POINT ( 'NONE',  ( -35.58475201036861080, -24.63419186844611986, 9.035850630976925757 ) ) ;
#55448=ORIENTED_EDGE ( 'NONE', *, *, #93635, .T. ) ;
#55449=EDGE_CURVE ( 'NONE', #1269, #991, #75035, .T. ) ;
#55450=CARTESIAN_POINT ( 'NONE',  ( -45.52287095715006160, -24.91570333825768913, 8.075032458260363200 ) ) ;
#55451=ORIENTED_EDGE ( 'NONE', *, *, #77896, .T. ) ;
#55452=VECTOR ( 'NONE', #56234, 1000.000000000000114 ) ;
#55453=CARTESIAN_POINT ( 'NONE',  ( -100.6228709571500701, -23.47596703998600631, 11.44779298504227860 ) ) ;
#55454=CARTESIAN_POINT ( 'NONE',  ( 3.105769797727405024, 20.95935918496786599, -1.500000000000002220 ) ) ;
#55455=B_SPLINE_CURVE_WITH_KNOTS ( 'NONE', 3,
 ( #80299, #50859, #58475, #81796, #95523, #33629 ),
 .UNSPECIFIED., .F., .F.,
 ( 4, 2, 4 ),
 ( 0.000000000000000000, 0.001380901958385388545, 0.002761803916770777089 ),
 .UNSPECIFIED. ) ;
#55456=ORIENTED_EDGE ( 'NONE', *, *, #72142, .F. ) ;
#55457=CARTESIAN_POINT ( 'NONE',  ( -50.52198866362500240, -23.48783264082477018, -1.443836473390096797 ) ) ;
#55458=CARTESIAN_POINT ( 'NONE',  ( -19.95566455537076678, 8.849265345510103131, -1.500000000000002220 ) ) ;
#55459=DIRECTION ( 'NONE',  ( 3.773278334444167608E-23, -1.000000000000000000, 0.000000000000000000 ) ) ;
#55460=B_SPLINE_CURVE_WITH_KNOTS ( 'NONE', 3,
 ( #99341, #83622, #21709, #52683 ),
 .UNSPECIFIED., .F., .F.,
 ( 4, 4 ),
 ( 0.02051464900870706917, 0.02952108028082290475 ),
 .UNSPECIFIED. ) ;
#55461=CARTESIAN_POINT ( 'NONE',  ( -62.55620429048339304, -24.66019654487199020, 8.947790411086131712 ) ) ;
#55463=CARTESIAN_POINT ( 'NONE',  ( -6.457742198559264679, -20.83860622980983024, -1.500000000000002220 ) ) ;
#55465=VERTEX_POINT ( 'NONE', #46136 ) ;
#55466=CARTESIAN_POINT ( 'NONE',  ( -41.62287095715007723, -24.50216790748204687, 0.6166512839542525048 ) ) ;
#55467=CARTESIAN_POINT ( 'NONE',  ( -48.87380231474225667, -25.12782503098429743, 6.137092279293525188 ) ) ;
#55468=VERTEX_POINT ( 'NONE', #69466 ) ;
#55469=CARTESIAN_POINT ( 'NONE',  ( -129.5222683580481089, -23.48786465467241769, 11.44779295918253759 ) ) ;
#55470=ORIENTED_EDGE ( 'NONE', *, *, #99672, .T. ) ;
#55471=ORIENTED_EDGE ( 'NONE', *, *, #31686, .T. ) ;
#55473=DIRECTION ( 'NONE',  ( -3.773278334453079030E-23, 0.9999999999976377785, 2.173523156925979128E-06 ) ) ;
#55474=CARTESIAN_POINT ( 'NONE',  ( -113.6228709571500559, -24.65952944569304961, 1.056160979905706565 ) ) ;
#55475=CARTESIAN_POINT ( 'NONE',  ( 1.624102159173431259, 21.17561035156254334, -1.500000000000002220 ) ) ;
#55478=CARTESIAN_POINT ( 'NONE',  ( -41.55620429048340014, -24.65952944569304606, 1.056160979905691910 ) ) ;
#55480=CARTESIAN_POINT ( 'NONE',  ( -127.5895376238166961, -24.66019654487200086, 8.947790411086117501 ) ) ;
#55481=CARTESIAN_POINT ( 'NONE',  ( 8.513215801882951794, -17.43586836189350819, 11.49999999999998934 ) ) ;
#55482=CARTESIAN_POINT ( 'NONE',  ( -117.5893256543061653, -24.35071581493544457, 9.817618358456019934 ) ) ;
#55483=ORIENTED_EDGE ( 'NONE', *, *, #95316, .F. ) ;
#55484=CARTESIAN_POINT ( 'NONE',  ( -12.10551386448753064, 15.32171617432465816, 11.49999999999999645 ) ) ;
#55486=CARTESIAN_POINT ( 'NONE',  ( -79.39961074542060260, -25.23283802384501584, 6.332283618388551361 ) ) ;
#55487=ORIENTED_EDGE ( 'NONE', *, *, #49097, .T. ) ;
#55488=CARTESIAN_POINT ( 'NONE',  ( -98.62287095715005592, -24.66019654487199730, 8.947790411086124607 ) ) ;
#55489=CARTESIAN_POINT ( 'NONE',  ( -89.54581868124135724, -24.51314013834317862, 0.6176544820404262781 ) ) ;
#55490=FACE_OUTER_BOUND ( 'NONE', #76485, .T. ) ;
#55493=CARTESIAN_POINT ( 'NONE',  ( -16.89733858281218204, -10.06102416988892934, -1.500000000000002220 ) ) ;
#55496=CARTESIAN_POINT ( 'NONE',  ( 20.55510029441247610, -6.647428040031946317, -1.500000000000002220 ) ) ;
#55497=B_SPLINE_CURVE_WITH_KNOTS ( 'NONE', 3,
 ( #24995, #62079, #93003, #54965 ),
 .UNSPECIFIED., .F., .F.,
 ( 4, 4 ),
 ( 0.000000000000000000, 8.007323677445510822E-05 ),
 .UNSPECIFIED. ) ;
#55498=CARTESIAN_POINT ( 'NONE',  ( -100.6814946224345846, -29.50249428492551829, 5.197779886230994073 ) ) ;
#55500=B_SPLINE_CURVE_WITH_KNOTS ( 'NONE', 3,
 ( #82804, #51373, #75192, #5686, #12790, #43760, #59992, #45258, #29516, #74693, #75685, #5188, #21891, #76184, #36636, #36145, #6683, #67604, #98522, #68592, #90924, #83303 ),
 .UNSPECIFIED., .F., .F.,
 ( 4, 2, 2, 2, 2, 2, 2, 2, 2, 2, 4 ),
 ( 0.000000000000000000, 0.0002773043728616134650, 0.0005546087457232269299, 0.0008319131185848405033, 0.001109217491446453860, 0.001663826237169669514, 0.002218434982892885168, 0.002773043728616100823, 0.003327652474339316043, 0.003882261220062532131, 0.004436869965785747785 ),
 .UNSPECIFIED. ) ;
#55501=CARTESIAN_POINT ( 'NONE',  ( 11.75533340255842596, 19.88161105567325038, -1.500000000000002220 ) ) ;
#55505=DIRECTION ( 'NONE',  ( -3.773278334444166432E-23, 1.000000000000000000, 0.000000000000000000 ) ) ;
#55509=CARTESIAN_POINT ( 'NONE',  ( -110.7466941838547143, -25.10921386403298072, 2.889691385203864371 ) ) ;
#55510=CARTESIAN_POINT ( 'NONE',  ( -121.6228709571500985, -24.35013146730204525, 9.818937971375104823 ) ) ;
#55512=CARTESIAN_POINT ( 'NONE',  ( -114.5520155267526832, -24.51419770103158768, 9.386484678747160970 ) ) ;
#55513=CARTESIAN_POINT ( 'NONE',  ( -18.69216024341242743, -6.879743215651725308, 11.49999999999998934 ) ) ;
#55514=EDGE_CURVE ( 'NONE', #18750, #85588, #83485, .T. ) ;
#55516=CARTESIAN_POINT ( 'NONE',  ( -75.60360349675073621, -23.85049219812685806, 10.88485053497527488 ) ) ;
#55517=CARTESIAN_POINT ( 'NONE',  ( 4.164567180745167185, 19.39263604865329071, -1.500000000000002220 ) ) ;
#55519=CARTESIAN_POINT ( 'NONE',  ( -71.62287095715005592, -23.47593901973091235, -1.443836447539006196 ) ) ;
#55520=EDGE_CURVE ( 'NONE', #69268, #2927, #79576, .T. ) ;
#55522=CARTESIAN_POINT ( 'NONE',  ( -39.14342005660770241, -25.10925777441851992, 3.683763713153402897 ) ) ;
#55523=DIRECTION ( 'NONE',  ( -3.773278334453079030E-23, 0.9999999999976377785, 2.173523156925979128E-06 ) ) ;
#55524=CARTESIAN_POINT ( 'NONE',  ( 1.902724757927627408, 20.64897553884969028, 11.49999999999999645 ) ) ;
#55527=PLANE ( 'NONE',  #11708 ) ;
#55528=CARTESIAN_POINT ( 'NONE',  ( -18.67006117854901959, 13.05921059288911934, 11.49999999999999645 ) ) ;
#55529=VECTOR ( 'NONE', #57495, 1000.000000000000114 ) ;
#55530=VERTEX_POINT ( 'NONE', #25792 ) ;
#55531=B_SPLINE_SURFACE_WITH_KNOTS ( 'NONE', 3, 3, ( 
 ( #40384, #71336, #85545, #77420 ),
 ( #79433, #8923, #1826, #48505 ),
 ( #314, #46994, #39377, #31258 ),
 ( #9924, #7923, #78426, #38871 ),
 ( #77917, #39876, #814, #31767 ),
 ( #62736, #93652, #1326, #71838 ),
 ( #35277, #40879, #66241, #87554 ),
 ( #25651, #50009, #88061, #42403 ),
 ( #19034, #2330, #81447, #50494 ),
 ( #3830, #58607, #96662, #18039 ),
 ( #64245, #88560, #33259, #65741 ),
 ( #96173, #72341, #56625, #80943 ),
 ( #27158, #97167, #11428, #34276 ),
 ( #4327, #79935, #95167, #41898 ),
 ( #58122, #72841, #81936, #2833 ),
 ( #33770, #49004, #10423, #41385 ),
 ( #65249, #27661, #26659, #64752 ),
 ( #11926, #57620, #89059, #42890 ),
 ( #73826, #73337, #89553, #19532 ),
 ( #20037, #95669, #51001, #26151 ),
 ( #57125, #34771, #18538, #49506 ),
 ( #80442, #10931, #3340, #35772 ),
 ( #98645, #30136, #51993, #6310 ),
 ( #92038, #22010, #52493, #66741 ),
 ( #59114, #29144, #52999, #75808 ) ),
 .UNSPECIFIED., .F., .F., .F.,
 ( 4, 3, 3, 3, 3, 3, 3, 3, 4 ),
 ( 4, 4 ),
 ( -7.445425705058654331E-16, 0.1249999999999994726, 0.1874999999999995837, 0.2499999999999996947, 0.5000000000000001110, 0.7500000000000004441, 0.8125000000000005551, 0.8750000000000006661, 1.000000000000000888 ),
 ( 0.000000000000000000, 1.000000000000000000 ),
 .UNSPECIFIED. ) ;
#55532=CARTESIAN_POINT ( 'NONE',  ( -69.55396335837851041, -23.96119346886880663, -0.6495511937832122440 ) ) ;
#55534=VERTEX_POINT ( 'NONE', #88200 ) ;
#55535=CARTESIAN_POINT ( 'NONE',  ( -0.5548696950099620828, -20.20177982057877841, 11.49999999999998934 ) ) ;
#55539=EDGE_LOOP ( 'NONE', ( #26500, #31639, #15567, #64735 ) ) ;
#55540=CARTESIAN_POINT ( 'NONE',  ( -0.1490770655183801252, -21.12008023607309681, -1.443836447538997758 ) ) ;
#55541=CARTESIAN_POINT ( 'NONE',  ( 5.768980952343642166, -22.17701263744951490, -1.500000000000002220 ) ) ;
#55542=CARTESIAN_POINT ( 'NONE',  ( -100.6228709571500559, -24.99132157543167310, 2.256160258750667502 ) ) ;
#55543=CARTESIAN_POINT ( 'NONE',  ( -19.89792590360708147, -2.209704250470923892, -1.500000000000002220 ) ) ;
#55546=CARTESIAN_POINT ( 'NONE',  ( 0.9685562702117149758, 20.96446713366763248, 11.49999999999999645 ) ) ;
#55548=CARTESIAN_POINT ( 'NONE',  ( -69.03429854110324015, -25.24754422676405241, 5.665244721077478118 ) ) ;
#55549=CARTESIAN_POINT ( 'NONE',  ( -10.85839155550747392, 19.17434714687634667, 11.49999999999998934 ) ) ;
#55550=CARTESIAN_POINT ( 'NONE',  ( -101.9228709571500815, -23.47593901973090524, -1.443836447538996870 ) ) ;
#55551=ORIENTED_EDGE ( 'NONE', *, *, #91533, .F. ) ;
#55553=FACE_OUTER_BOUND ( 'NONE', #38862, .T. ) ;
#55554=ORIENTED_EDGE ( 'NONE', *, *, #35448, .T. ) ;
#55555=DIRECTION ( 'NONE',  ( 0.000000000000000000, -0.9999999999976377785, -2.173523156925979975E-06 ) ) ;
#55556=ORIENTED_EDGE ( 'NONE', *, *, #38762, .T. ) ;
#55558=CARTESIAN_POINT ( 'NONE',  ( -118.6228709571500559, -24.66019654487200086, 8.947790411086117501 ) ) ;
#55561=CARTESIAN_POINT ( 'NONE',  ( 18.12345787009687115, -9.690629616749632191, -1.500000000000002220 ) ) ;
#55562=EDGE_CURVE ( 'NONE', #33349, #51268, #33898, .T. ) ;
#55563=ORIENTED_EDGE ( 'NONE', *, *, #11803, .F. ) ;
#55564=CARTESIAN_POINT ( 'NONE',  ( -100.5246099931740105, -25.30387691067383926, 5.206566059064181573 ) ) ;
#55567=CARTESIAN_POINT ( 'NONE',  ( -21.97457344801873447, 3.670769625195870134, -1.500000000000002220 ) ) ;
#55570=CARTESIAN_POINT ( 'NONE',  ( -80.52287095715006160, -23.47596703998600631, 11.44779298504228571 ) ) ;
#55571=CARTESIAN_POINT ( 'NONE',  ( -26.11966125959963847, -24.71873968571609836, 7.419517041710707694 ) ) ;
#55572=ORIENTED_EDGE ( 'NONE', *, *, #54572, .T. ) ;
#55573=CARTESIAN_POINT ( 'NONE',  ( -29.81066356762512726, -25.24533126392478266, 4.756803792137969999 ) ) ;
#55576=CARTESIAN_POINT ( 'NONE',  ( -12.81329989551134751, 16.42372500408851366, 11.49999999999998934 ) ) ;
#55577=ORIENTED_EDGE ( 'NONE', *, *, #15111, .T. ) ;
#55579=ORIENTED_EDGE ( 'NONE', *, *, #47520, .T. ) ;
#55581=VECTOR ( 'NONE', #85570, 1000.000000000000227 ) ;
#55583=CARTESIAN_POINT ( 'NONE',  ( 16.07406896385161943, -13.52096256729613266, -1.500000000000002220 ) ) ;
#55584=EDGE_CURVE ( 'NONE', #56477, #51806, #27787, .T. ) ;
#55585=VERTEX_POINT ( 'NONE', #50137 ) ;
#55586=CARTESIAN_POINT ( 'NONE',  ( -110.6228709571500417, -24.14321612903117753, -0.2833117244520985123 ) ) ;
#55587=CARTESIAN_POINT ( 'NONE',  ( -49.74369414166532266, -25.30543060587212167, 4.940877950953177944 ) ) ;
#55590=CARTESIAN_POINT ( 'NONE',  ( -101.4365978186105366, -25.25419481222983720, 7.227288580716594524 ) ) ;
#55591=CARTESIAN_POINT ( 'NONE',  ( -66.52287095715006160, -29.50248528299804818, 1.056150453629036701 ) ) ;
#55592=DIRECTION ( 'NONE',  ( 0.000000000000000000, 2.173523156925980399E-06, -0.9999999999976378895 ) ) ;
#55593=CARTESIAN_POINT ( 'NONE',  ( -20.66209241242137296, -8.185968977665980972, 11.49999999999999645 ) ) ;
#55596=ADVANCED_FACE ( 'NONE', ( #80576 ), #49850, .T. ) ;
#55597=DIRECTION ( 'NONE',  ( -3.773278334453080206E-23, 0.9999999999976377785, 2.173523156925979975E-06 ) ) ;
#55599=CARTESIAN_POINT ( 'NONE',  ( 16.59953334139655468, -15.42474913338910980, -1.500000000000002220 ) ) ;
#55600=CARTESIAN_POINT ( 'NONE',  ( -76.62287095715002749, -24.33832256526968507, 0.1851278514119898688 ) ) ;
#55601=ORIENTED_EDGE ( 'NONE', *, *, #87319, .F. ) ;
#55604=B_SPLINE_CURVE_WITH_KNOTS ( 'NONE', 3,
 ( #93438, #24934, #55404, #69623 ),
 .UNSPECIFIED., .F., .F.,
 ( 4, 4 ),
 ( 0.000000000000000000, 9.999999999998897304E-05 ),
 .UNSPECIFIED. ) ;
#55606=CARTESIAN_POINT ( 'NONE',  ( 16.24926901856429140, 11.90123039513101411, -1.500000000000002220 ) ) ;
#55608=ORIENTED_EDGE ( 'NONE', *, *, #59809, .T. ) ;
#55610=CARTESIAN_POINT ( 'NONE',  ( -87.52287095715006160, -29.50250243563736774, 8.947779886222139822 ) ) ;
#55611=CARTESIAN_POINT ( 'NONE',  ( -3.695635658436464244, 22.08213133993951161, -1.500000000000002220 ) ) ;
#55612=ORIENTED_EDGE ( 'NONE', *, *, #13559, .F. ) ;
#55613=ORIENTED_EDGE ( 'NONE', *, *, #67213, .F. ) ;
#55616=CARTESIAN_POINT ( 'NONE',  ( -94.51279141762005054, -24.15620529776628089, 10.23563542870660470 ) ) ;
#55620=B_SPLINE_CURVE_WITH_KNOTS ( 'NONE', 3,
 ( #14913, #45887, #76802, #49281 ),
 .UNSPECIFIED., .F., .F.,
 ( 4, 4 ),
 ( 0.4300930433922509066, 0.4390994746643664959 ),
 .UNSPECIFIED. ) ;
#55621=CARTESIAN_POINT ( 'NONE',  ( 7.829539893445508270, 17.95258299782629408, -1.500000000000002220 ) ) ;
#55625=CARTESIAN_POINT ( 'NONE',  ( 2.564635614221720594, -21.35862533600356983, 11.49999999999998934 ) ) ;
#55626=CARTESIAN_POINT ( 'NONE',  ( -128.5898165004505813, -24.15543982623908548, -0.2315651400026392803 ) ) ;
#55629=CARTESIAN_POINT ( 'NONE',  ( -111.6228709571500843, -24.34917612406838572, 0.1852690917426694506 ) ) ;
#55630=CARTESIAN_POINT ( 'NONE',  ( 10.67403711042701353, -20.27515232684288549, -1.500000000000002220 ) ) ;
#55632=CARTESIAN_POINT ( 'NONE',  ( -92.52287095715006160, -23.47593901973090169, -1.443836447538996426 ) ) ;
#55633=CARTESIAN_POINT ( 'NONE',  ( -53.61318609310688288, -23.48783264082475952, -1.443836473390095909 ) ) ;
#55634=CARTESIAN_POINT ( 'NONE',  ( 18.34943919012036773, 8.063251210807163005, 11.49999999999999645 ) ) ;
#55635=CARTESIAN_POINT ( 'NONE',  ( -80.35919894935766195, -25.31594315932206385, 4.505481293487486383 ) ) ;
#55641=CARTESIAN_POINT ( 'NONE',  ( 11.36066313177254905, -18.55813952095733654, 11.49999999999998934 ) ) ;
#55642=CARTESIAN_POINT ( 'NONE',  ( -71.62287095715005592, -29.50248528299804818, 1.056150453629036701 ) ) ;
#55643=CARTESIAN_POINT ( 'NONE',  ( 18.24227566675094181, -7.298356753547692755, -1.500000000000002220 ) ) ;
#55644=CARTESIAN_POINT ( 'NONE',  ( -122.6228709571500701, -23.48783264082479505, -1.443836473390058828 ) ) ;
#55645=B_SPLINE_CURVE_WITH_KNOTS ( 'NONE', 3,
 ( #84565, #15051, #76940, #38393, #85063, #79454 ),
 .UNSPECIFIED., .F., .F.,
 ( 4, 2, 4 ),
 ( 0.000000000000000000, 0.001380764517854767134, 0.002761529035709534268 ),
 .UNSPECIFIED. ) ;
#55647=CARTESIAN_POINT ( 'NONE',  ( -110.2093792378191921, -25.27925965549014009, 5.585409257837866903 ) ) ;
#55648=EDGE_CURVE ( 'NONE', #67134, #38032, #19326, .T. ) ;
#55649=DIRECTION ( 'NONE',  ( 1.000000000000000000, 3.773278334444167608E-23, 8.201307833595939069E-29 ) ) ;
#55650=CARTESIAN_POINT ( 'NONE',  ( -30.57287095715006231, -23.47593901973084485, -1.443836476861628304 ) ) ;
#55651=CARTESIAN_POINT ( 'NONE',  ( -7.762539992054180438, 19.06225842855939234, 11.49999999999999645 ) ) ;
#55653=ADVANCED_FACE ( 'NONE', ( #20166 ), #91670, .T. ) ;
#55656=CARTESIAN_POINT ( 'NONE',  ( 21.16457415087624128, -7.944649954575952577, 11.49999999999999645 ) ) ;
#55658=CARTESIAN_POINT ( 'NONE',  ( 0.000000000000000000, 0.000000000000000000, 0.000000000000000000 ) ) ;
#55659=CARTESIAN_POINT ( 'NONE',  ( -70.22494714645260672, -25.25639600851938837, 7.098707166320516571 ) ) ;
#55660=CARTESIAN_POINT ( 'NONE',  ( -27.08767087237659865, -24.79334963567931283, 7.466528724393665328 ) ) ;
#55661=CARTESIAN_POINT ( 'NONE',  ( -108.5228709571500758, -23.48783264083353473, -1.443836473376470586 ) ) ;
#55662=CARTESIAN_POINT ( 'NONE',  ( -85.62287095715002749, -24.63287334234178516, 0.9662140553045440727 ) ) ;
#55664=ADVANCED_FACE ( 'NONE', ( #14042 ), #12589, .T. ) ;
#55665=CARTESIAN_POINT ( 'NONE',  ( -26.35953173686715800, -24.93063513829692823, 7.694642102573395093 ) ) ;
#55668=CARTESIAN_POINT ( 'NONE',  ( -79.34772585426964042, -25.26750084320114453, 5.924311888455177311 ) ) ;
#55669=CARTESIAN_POINT ( 'NONE',  ( -22.75767140345847750, 1.815691853630000629, -1.500000000000002220 ) ) ;
#55670=CARTESIAN_POINT ( 'NONE',  ( -125.5562042904834215, -25.00158670708909980, 2.256160236439166855 ) ) ;
#55671=B_SPLINE_SURFACE_WITH_KNOTS ( 'NONE', 3, 1, ( 
 ( #6429, #99265 ),
 ( #86044, #6921 ),
 ( #15025, #31762 ),
 ( #46487, #46990 ),
 ( #31253, #45995 ),
 ( #30756, #37383 ),
 ( #60729, #76916 ),
 ( #69321, #309 ),
 ( #77913, #62728 ),
 ( #7415, #8421 ),
 ( #61728, #55108 ) ),
 .UNSPECIFIED., .F., .F., .F.,
 ( 4, 1, 1, 1, 1, 1, 1, 1, 4 ),
 ( 2, 2 ),
 ( 0.000000000000000000, 0.1497703860319676283, 0.2913164099952436636, 0.4259663731047447777, 0.5521595739695276395, 0.6715274135235875796, 0.7861216286916553608, 0.8953250730704447324, 1.000000000000000000 ),
 ( 0.000000000000000000, 1.000000000000000000 ),
 .UNSPECIFIED. ) ;
#55672=CARTESIAN_POINT ( 'NONE',  ( -115.5228709571500758, -24.91570333825770689, 8.075032458260366752 ) ) ;
#55673=CARTESIAN_POINT ( 'NONE',  ( -63.55375729026285825, -23.96169478059713143, 10.65365249895718236 ) ) ;
#55674=CARTESIAN_POINT ( 'NONE',  ( 0.003324065884441271702, 22.49086686382009503, 11.49999999999999645 ) ) ;
#55675=VERTEX_POINT ( 'NONE', #13049 ) ;
#55677=CARTESIAN_POINT ( 'NONE',  ( -21.49438740719132923, 4.340694165963498996, -1.500000000000002220 ) ) ;
#55678=CARTESIAN_POINT ( 'NONE',  ( -124.7735373858569403, -25.37153787860454557, 4.078969152973343171 ) ) ;
#55679=CARTESIAN_POINT ( 'NONE',  ( -34.63526505597382510, -24.35071581493542681, 9.817618358456032368 ) ) ;
#55680=DIRECTION ( 'NONE',  ( -3.773278334453079030E-23, 0.9999999999976377785, 2.173523156925979128E-06 ) ) ;
#55681=ORIENTED_EDGE ( 'NONE', *, *, #22985, .F. ) ;
#55682=CARTESIAN_POINT ( 'NONE',  ( -48.59960390203813319, -23.96169478059712787, 10.65365249895718236 ) ) ;
#55683=CARTESIAN_POINT ( 'NONE',  ( -111.5228709571500616, -23.48786465467242479, 11.44779295918253936 ) ) ;
#55685=CARTESIAN_POINT ( 'NONE',  ( -11.47117155886032158, -16.94740806926979815, 11.49999999999998934 ) ) ;
#55686=VERTEX_POINT ( 'NONE', #51128 ) ;
#55687=B_SPLINE_CURVE_WITH_KNOTS ( 'NONE', 3,
 ( #72135, #8725, #17838, #85329, #32052, #54399, #86835, #78214, #63024, #48291, #54901, #24435, #94453, #24935, #77709, #2125, #56417, #23415 ),
 .UNSPECIFIED., .F., .F.,
 ( 4, 2, 2, 2, 2, 2, 2, 2, 4 ),
 ( 2.602085213965210642E-18, 0.0005889077912318151520, 0.001177815582463627702, 0.001766723373695440469, 0.002355631164927252802, 0.002944538956159065135, 0.003533446747390878336, 0.004122354538622689801, 0.004711262329854501267 ),
 .UNSPECIFIED. ) ;
#55688=ORIENTED_EDGE ( 'NONE', *, *, #97883, .F. ) ;
#55689=VERTEX_POINT ( 'NONE', #67359 ) ;
#55691=CARTESIAN_POINT ( 'NONE',  ( 22.94779996701378266, 2.684060219229261968, 11.49999999999998934 ) ) ;
#55692=CARTESIAN_POINT ( 'NONE',  ( -41.47713460189704193, -25.30977039686255026, 4.487062071701387822 ) ) ;
#55693=CARTESIAN_POINT ( 'NONE',  ( 14.61151973098085222, 14.07909450314327771, -1.500000000000002220 ) ) ;
#55696=DIRECTION ( 'NONE',  ( 0.000000000000000000, -0.9999999999976377785, -2.173523156925979975E-06 ) ) ;
#55697=CARTESIAN_POINT ( 'NONE',  ( -92.62357504500812411, -24.65952944569303895, 1.056160979905702346 ) ) ;
#55698=EDGE_CURVE ( 'NONE', #69040, #83981, #96795, .T. ) ;
#55699=FACE_OUTER_BOUND ( 'NONE', #13203, .T. ) ;
#55701=CARTESIAN_POINT ( 'NONE',  ( -18.34654256122676941, -11.15389649534839833, 11.49999999999999645 ) ) ;
#55702=ORIENTED_EDGE ( 'NONE', *, *, #15863, .T. ) ;
#55703=CARTESIAN_POINT ( 'NONE',  ( -75.50777110636425959, -24.15503026093913519, -0.2815557561904521444 ) ) ;
#55704=CARTESIAN_POINT ( 'NONE',  ( -112.5895376238167245, -24.64898659630368272, 1.056161002820390493 ) ) ;
#55707=CARTESIAN_POINT ( 'NONE',  ( 16.28047541435887879, -12.87082401369967677, 11.49999999999998934 ) ) ;
#55708=VERTEX_POINT ( 'NONE', #43523 ) ;
#55709=EDGE_CURVE ( 'NONE', #60813, #8894, #91927, .T. ) ;
#55710=CARTESIAN_POINT ( 'NONE',  ( -125.5549482276435640, -24.52300882791529801, 0.6510814631126508045 ) ) ;
#55712=CARTESIAN_POINT ( 'NONE',  ( -111.5868581930692329, -24.66019654487200441, 8.947790411086105067 ) ) ;
#55717=FACE_OUTER_BOUND ( 'NONE', #6007, .T. ) ;
#55718=CARTESIAN_POINT ( 'NONE',  ( -43.48725217974529045, -24.51419770103157347, 9.386484678747182286 ) ) ;
#55719=CARTESIAN_POINT ( 'NONE',  ( 2.156995527713877259, 21.93451973775924557, 11.49999999999999645 ) ) ;
#55720=VERTEX_POINT ( 'NONE', #76439 ) ;
#55722=CARTESIAN_POINT ( 'NONE',  ( -22.20892344277460850, -4.061126821146308963, 11.49999999999998934 ) ) ;
#55723=CARTESIAN_POINT ( 'NONE',  ( 16.07406896385161943, -13.52096256729613266, 11.49999999999998934 ) ) ;
#55725=VERTEX_POINT ( 'NONE', #75440 ) ;
#55727=CARTESIAN_POINT ( 'NONE',  ( -59.62287095715005592, -24.33927499327854704, 9.819080762295818943 ) ) ;
#55730=CARTESIAN_POINT ( 'NONE',  ( -114.5895376238167245, -23.47593901973091235, -1.443836447538999312 ) ) ;
#55731=ORIENTED_EDGE ( 'NONE', *, *, #6602, .F. ) ;
#55732=CARTESIAN_POINT ( 'NONE',  ( -3.482456173223098528, 20.84670800329844198, -1.500000000000002220 ) ) ;
#55733=CARTESIAN_POINT ( 'NONE',  ( -66.62287095715002749, -23.95044443724991368, 10.65354141964649592 ) ) ;
#55734=CARTESIAN_POINT ( 'NONE',  ( -59.79108751027236934, -25.31249728293746060, 5.276660823416808199 ) ) ;
#55735=CARTESIAN_POINT ( 'NONE',  ( -49.51573515180496798, -25.27160265537046513, 4.092660780511780061 ) ) ;
#55737=CARTESIAN_POINT ( 'NONE',  ( -35.62287095715005592, -29.50247984919015209, -1.443849546365060466 ) ) ;
#55738=CARTESIAN_POINT ( 'NONE',  ( 18.11909884760711975, -12.84011383348296853, -1.500000000000002220 ) ) ;
#55740=CARTESIAN_POINT ( 'NONE',  ( -114.5168412745318278, -24.34968618360934300, 0.1864209137778971848 ) ) ;
#55741=B_SPLINE_CURVE_WITH_KNOTS ( 'NONE', 3,
 ( #11674, #50756, #58375, #27419, #19782, #81701 ),
 .UNSPECIFIED., .F., .F.,
 ( 4, 2, 4 ),
 ( 3.087040877776988824E-09, 0.002715410320741953962, 0.005430817554443030659 ),
 .UNSPECIFIED. ) ;
#55743=CARTESIAN_POINT ( 'NONE',  ( -110.5228709571500616, -23.47596703998600631, 11.44779298504228038 ) ) ;
#55745=CARTESIAN_POINT ( 'NONE',  ( -126.5204133787001268, -24.65952944569306027, 1.056160979905708786 ) ) ;
#55747=CARTESIAN_POINT ( 'NONE',  ( -41.82789317813108454, -25.25077454730569571, 3.845825085393474563 ) ) ;
#55748=CARTESIAN_POINT ( 'NONE',  ( -0.1490749075164066184, -21.12010817310450861, 11.44779298504228038 ) ) ;
#55749=CARTESIAN_POINT ( 'NONE',  ( -2.678125609936932605, 19.29598960679622976, 11.49999999999998934 ) ) ;
#55750=CARTESIAN_POINT ( 'NONE',  ( -13.99230614532761052, -16.21612836239924960, -1.500000000000002220 ) ) ;
#55751=CARTESIAN_POINT ( 'NONE',  ( -126.6228709571500843, -24.65952944569305316, 1.056160979905707675 ) ) ;
#55752=CARTESIAN_POINT ( 'NONE',  ( -60.52202393459451457, -23.48786465467241413, 11.44779295918254824 ) ) ;
#55753=CARTESIAN_POINT ( 'NONE',  ( -51.58228013677727120, -24.51314013834315730, 0.6176544820404110681 ) ) ;
#55754=CARTESIAN_POINT ( 'NONE',  ( -38.55620429048340014, -24.65952944569303895, 1.056160979905691688 ) ) ;
#55755=CARTESIAN_POINT ( 'NONE',  ( 15.23092229589061830, -16.91372389758942418, -1.500000000000002220 ) ) ;
#55757=DIRECTION ( 'NONE',  ( 3.773278334444167608E-23, -1.000000000000000000, 0.000000000000000000 ) ) ;
#55758=CARTESIAN_POINT ( 'NONE',  ( -2.735935421901279696, -19.66989661884619522, 11.49999999999999645 ) ) ;
#55759=CARTESIAN_POINT ( 'NONE',  ( -123.5538537614054917, -24.66019654487200441, 8.947790411086106843 ) ) ;
#55760=CARTESIAN_POINT ( 'NONE',  ( -89.81226385320383088, -25.22391155068715207, 6.409327647370969494 ) ) ;
#55762=EDGE_CURVE ( 'NONE', #92089, #78003, #62754, .T. ) ;
#55763=ORIENTED_EDGE ( 'NONE', *, *, #50954, .F. ) ;
#55764=PLANE ( 'NONE',  #68816 ) ;
#55766=VECTOR ( 'NONE', #93450, 1000.000000000000114 ) ;
#55767=CARTESIAN_POINT ( 'NONE',  ( -51.04701396381788925, -25.27412261295166829, 2.986905721224212495 ) ) ;
#55768=CARTESIAN_POINT ( 'NONE',  ( -17.90551237062050305, -12.20792721910736667, -1.500000000000002220 ) ) ;
#55770=CARTESIAN_POINT ( 'NONE',  ( -7.499459838998954631, -17.95702976299720532, -1.500000000000002220 ) ) ;
#55771=FACE_OUTER_BOUND ( 'NONE', #78708, .T. ) ;
#55772=ORIENTED_EDGE ( 'NONE', *, *, #36047, .F. ) ;
#55773=VECTOR ( 'NONE', #38681, 1000.000000000000114 ) ;
#55774=CARTESIAN_POINT ( 'NONE',  ( 12.15263457413992576, -16.39098610538439615, 11.49999999999999645 ) ) ;
#55777=LINE ( 'NONE', #16688, #33506 ) ;
#55780=CARTESIAN_POINT ( 'NONE',  ( -0.1426030150137709285, -21.20389190742572083, 11.50200000000000422 ) ) ;
#55782=CARTESIAN_POINT ( 'NONE',  ( -39.04762117679405264, -25.27985297379428786, 4.358277487482919987 ) ) ;
#55785=CARTESIAN_POINT ( 'NONE',  ( 7.746586651691365510, 18.53313339873204058, -1.500000000000002220 ) ) ;
#55790=DIRECTION ( 'NONE',  ( -3.773278334453079618E-23, 0.9999999999976377785, 2.173523156925979975E-06 ) ) ;
#55791=ADVANCED_FACE ( 'NONE', ( #93167 ), #92669, .T. ) ;
#55792=CARTESIAN_POINT ( 'NONE',  ( -16.88208375265294237, -15.58181570610299715, 11.49999999999999645 ) ) ;
#55793=CARTESIAN_POINT ( 'NONE',  ( 22.67573665902413182, 1.879276792517311501, -1.500000000000002220 ) ) ;
#55795=CARTESIAN_POINT ( 'NONE',  ( -53.62287095715007013, -23.96177878511307568, 10.65340807706330217 ) ) ;
#55796=CARTESIAN_POINT ( 'NONE',  ( -91.52287095715006160, -23.48786465467241769, 11.44779295918254292 ) ) ;
#55797=CARTESIAN_POINT ( 'NONE',  ( -90.63293755609211644, -24.40034930558990922, 0.3402023900116054045 ) ) ;
#55798=CARTESIAN_POINT ( 'NONE',  ( -61.35927065337961039, -25.05684680783174656, 7.499198447843678395 ) ) ;
#55799=CARTESIAN_POINT ( 'NONE',  ( -128.5894277638150243, -24.66019654487200441, 8.947790411086108620 ) ) ;
#55800=PLANE ( 'NONE',  #54164 ) ;
#55803=EDGE_LOOP ( 'NONE', ( #96347, #33927, #98486, #47955 ) ) ;
#55804=CARTESIAN_POINT ( 'NONE',  ( 14.85214116200856083, 13.97194181870810326, 11.49999999999998934 ) ) ;
#55805=ORIENTED_EDGE ( 'NONE', *, *, #23694, .F. ) ;
#55806=ORIENTED_EDGE ( 'NONE', *, *, #99542, .F. ) ;
#55807=CARTESIAN_POINT ( 'NONE',  ( -22.94451526424785115, -1.264959178018935315, -1.500000000000002220 ) ) ;
#55809=ORIENTED_EDGE ( 'NONE', *, *, #51494, .F. ) ;
#55810=CARTESIAN_POINT ( 'NONE',  ( -110.2414688702968135, -25.26454195069187136, 6.186385695411759755 ) ) ;
#55811=CARTESIAN_POINT ( 'NONE',  ( -101.5228709571500616, -24.50216790748205042, 0.6166512839542561686 ) ) ;
#55813=CARTESIAN_POINT ( 'NONE',  ( -29.58953762381673869, -24.58133133125748060, 1.056161285064568078 ) ) ;
#55814=CARTESIAN_POINT ( 'NONE',  ( -10.68834330497911189, 18.46263264838738039, 11.49999999999999645 ) ) ;
#55816=VERTEX_POINT ( 'NONE', #17052 ) ;
#55817=CARTESIAN_POINT ( 'NONE',  ( 1.019757120859956512, 22.21710203930399175, -1.500000000000002220 ) ) ;
#55818=CARTESIAN_POINT ( 'NONE',  ( 11.79242832063081892, -16.95861370568002613, -1.500000000000002220 ) ) ;
#55819=AXIS2_PLACEMENT_3D ( 'NONE', #85204, #8086, #98926 ) ;
#55823=CARTESIAN_POINT ( 'NONE',  ( -95.60349243063225799, -23.48786465467241058, 11.44779295918254469 ) ) ;
#55825=CARTESIAN_POINT ( 'NONE',  ( -112.2228709571500644, -23.47593901973090524, -1.443836447538996648 ) ) ;
#55826=VERTEX_POINT ( 'NONE', #70348 ) ;
#55827=CARTESIAN_POINT ( 'NONE',  ( -129.6228709571500417, -24.65952944569305316, 1.056160979905706121 ) ) ;
#55828=CARTESIAN_POINT ( 'NONE',  ( -71.30293871510559711, -25.23939882842460847, 6.270859370734599203 ) ) ;
#55829=CARTESIAN_POINT ( 'NONE',  ( 11.28189403632909915, 17.58240144430209995, -1.500000000000002220 ) ) ;
#55830=CARTESIAN_POINT ( 'NONE',  ( -12.45635911906152771, -17.91357634596933934, 11.49999999999999645 ) ) ;
#55834=CARTESIAN_POINT ( 'NONE',  ( 8.413247042826936806, 20.86129769029627923, 11.49999999999998934 ) ) ;
#55835=CARTESIAN_POINT ( 'NONE',  ( -118.6267491325727406, -23.96169478059713853, 10.65365249895717170 ) ) ;
#55837=CARTESIAN_POINT ( 'NONE',  ( -31.55620429048339304, -24.64965694238574656, 8.947790433994208925 ) ) ;
#55839=ORIENTED_EDGE ( 'NONE', *, *, #96034, .T. ) ;
#55840=ORIENTED_EDGE ( 'NONE', *, *, #69008, .F. ) ;
#55842=ORIENTED_EDGE ( 'NONE', *, *, #85741, .F. ) ;
#55844=CARTESIAN_POINT ( 'NONE',  ( -2.881439591185620319, 21.19155266312798958, -1.500000000000002220 ) ) ;
#55845=CARTESIAN_POINT ( 'NONE',  ( 3.752539591237177508, -22.04708138622333635, 11.49999999999999645 ) ) ;
#55848=CARTESIAN_POINT ( 'NONE',  ( 12.48895993392301307, -16.95307763291877379, -1.500000000000002220 ) ) ;
#55849=CARTESIAN_POINT ( 'NONE',  ( -30.59773033261084763, -24.76236165402489675, 8.640462295247353097 ) ) ;
#55850=CARTESIAN_POINT ( 'NONE',  ( -7.573260116017839216, 18.43532004384545786, -1.500000000000002220 ) ) ;
#55851=CARTESIAN_POINT ( 'NONE',  ( -50.62375381348867620, -25.00182538069146432, 7.747789668545041586 ) ) ;
#55854=CARTESIAN_POINT ( 'NONE',  ( -14.46940225681120396, -16.66540133702554272, -1.500000000000002220 ) ) ;
#55855=PLANE ( 'NONE',  #86860 ) ;
#55856=ORIENTED_EDGE ( 'NONE', *, *, #11961, .T. ) ;
#55857=CARTESIAN_POINT ( 'NONE',  ( -65.62561620482574654, -24.92592662359561473, 8.075495903017998245 ) ) ;
#55858=ADVANCED_FACE ( 'NONE', ( #73356 ), #18057, .T. ) ;
#55860=CARTESIAN_POINT ( 'NONE',  ( 9.770152518076534065, 18.40777400073588410, 11.49999999999999645 ) ) ;
#55861=EDGE_CURVE ( 'NONE', #63898, #22592, #47200, .T. ) ;
#55864=CARTESIAN_POINT ( 'NONE',  ( -128.6228709571500417, -23.47596703998600631, 11.44779298504227860 ) ) ;
#55868=CARTESIAN_POINT ( 'NONE',  ( -18.83571791729191958, -9.990160686573538840, -1.500000000000002220 ) ) ;
#55869=CARTESIAN_POINT ( 'NONE',  ( -73.62287095715005592, -29.50250243563736774, 8.947779886222143375 ) ) ;
#55870=CARTESIAN_POINT ( 'NONE',  ( -124.5228709571500616, -23.47593901973090524, -1.443836447538996204 ) ) ;
#55871=CARTESIAN_POINT ( 'NONE',  ( -68.62287095715004170, -24.66019654487199020, 8.947790411086131712 ) ) ;
#55872=CARTESIAN_POINT ( 'NONE',  ( -95.62287095715005592, -29.50248789122583659, 2.256150453626215580 ) ) ;
#55873=CARTESIAN_POINT ( 'NONE',  ( 20.52096793114426276, -9.243637136814692568, -1.500000000000002220 ) ) ;
#55874=CARTESIAN_POINT ( 'NONE',  ( -112.5562042904833930, -23.47593901973091235, -1.443836447538999312 ) ) ;
#55876=CARTESIAN_POINT ( 'NONE',  ( -79.47058872164218712, -25.30399138793138292, 4.798136881959892186 ) ) ;
#55878=CARTESIAN_POINT ( 'NONE',  ( 10.64064036176630879, -16.58286410872727146, 11.49999999999999645 ) ) ;
#55880=CARTESIAN_POINT ( 'NONE',  ( -39.62287095715005592, -24.64898659630366851, 1.056161002820819261 ) ) ;
#55881=ADVANCED_FACE ( 'NONE', ( #49025 ), #40897, .F. ) ;
#55883=ORIENTED_EDGE ( 'NONE', *, *, #68587, .F. ) ;
#55886=CARTESIAN_POINT ( 'NONE',  ( -101.6228709571500559, -29.50248528299804818, 1.056150453629042030 ) ) ;
#55887=CARTESIAN_POINT ( 'NONE',  ( -95.52287095715010423, -25.00182538069145366, 7.747789668545101982 ) ) ;
#55889=CARTESIAN_POINT ( 'NONE',  ( 19.74453702311487646, -0.1846442961375113490, -1.500000000000002220 ) ) ;
#55890=ORIENTED_EDGE ( 'NONE', *, *, #67772, .F. ) ;
#55891=CARTESIAN_POINT ( 'NONE',  ( -5.148175472751820081, -19.54457232503198227, 11.49999999999999645 ) ) ;
#55896=DIRECTION ( 'NONE',  ( 0.000000000000000000, 2.173523156925980399E-06, -0.9999999999976378895 ) ) ;
#55897=CARTESIAN_POINT ( 'NONE',  ( -70.29603126573300642, -25.30156935299296350, 5.315006326144771087 ) ) ;
#55900=CARTESIAN_POINT ( 'NONE',  ( -124.5228709571500616, -23.47593901973090524, -1.443836447538996204 ) ) ;
#55901=CARTESIAN_POINT ( 'NONE',  ( -61.52287095715006160, -24.65952944569304606, 1.056160979905695463 ) ) ;
#55902=CARTESIAN_POINT ( 'NONE',  ( 19.27460657395150889, -5.330843762518559181, 11.49999999999998934 ) ) ;
#55903=EDGE_CURVE ( 'NONE', #47315, #37803, #43607, .T. ) ;
#55905=CARTESIAN_POINT ( 'NONE',  ( -67.62287095715005592, -23.48783264082478794, -1.443836473390067265 ) ) ;
#55906=CARTESIAN_POINT ( 'NONE',  ( -116.5166189026680570, -24.51419770103160189, 9.386484678747169852 ) ) ;
#55908=EDGE_CURVE ( 'NONE', #65310, #79871, #25161, .T. ) ;
#55909=EDGE_CURVE ( 'NONE', #3731, #24383, #56138, .T. ) ;
#55910=CARTESIAN_POINT ( 'NONE',  ( -79.64188460053713925, -23.73791477778911840, 11.05961554403170943 ) ) ;
#55911=CARTESIAN_POINT ( 'NONE',  ( -35.57399695948890184, -24.92564183028978775, 1.928384488918258199 ) ) ;
#55914=CARTESIAN_POINT ( 'NONE',  ( -45.62287095715004881, -29.50248789122583659, 2.256150453626215580 ) ) ;
#55915=DIRECTION ( 'NONE',  ( 1.000000000000000000, 3.773278334444167608E-23, 8.201307833595939069E-29 ) ) ;
#55917=CARTESIAN_POINT ( 'NONE',  ( -59.62287095715004881, -29.50247984919015209, -1.443849546365056913 ) ) ;
#55918=ORIENTED_EDGE ( 'NONE', *, *, #49822, .F. ) ;
#55919=CARTESIAN_POINT ( 'NONE',  ( 9.670762957215185196, 17.83519281925787325, -1.500000000000002220 ) ) ;
#55921=CARTESIAN_POINT ( 'NONE',  ( -34.58067719238572124, -24.51314013834315375, 0.6176544820404091807 ) ) ;
#55923=VERTEX_POINT ( 'NONE', #2854 ) ;
#55924=DIRECTION ( 'NONE',  ( 0.000000000000000000, -2.173523156925979552E-06, 0.9999999999976378895 ) ) ;
#55925=CARTESIAN_POINT ( 'NONE',  ( -4.116507902937485142, 19.75820112358731251, -1.500000000000002220 ) ) ;
#55926=CARTESIAN_POINT ( 'NONE',  ( 8.100108036306837178, -19.54698220168213041, 11.49999999999999645 ) ) ;
#55928=CARTESIAN_POINT ( 'NONE',  ( 21.13975321936677787, -6.629177502137091338, 11.49999999999998934 ) ) ;
#55929=CARTESIAN_POINT ( 'NONE',  ( -19.86366060283327784, 5.362777492974458049, -1.500000000000002220 ) ) ;
#55931=ORIENTED_EDGE ( 'NONE', *, *, #64959, .T. ) ;
#55932=CARTESIAN_POINT ( 'NONE',  ( -94.58953762381672448, -24.66019654487198665, 8.947790411086135265 ) ) ;
#55935=CARTESIAN_POINT ( 'NONE',  ( -34.52287095715006160, -29.50248528299804818, 1.056150453629029817 ) ) ;
#55936=ORIENTED_EDGE ( 'NONE', *, *, #31323, .F. ) ;
#55939=CARTESIAN_POINT ( 'NONE',  ( -110.4120913896815352, -25.12089013549993410, 2.834570756958135540 ) ) ;
#55940=FACE_OUTER_BOUND ( 'NONE', #22605, .T. ) ;
#55942=CARTESIAN_POINT ( 'NONE',  ( -1.268444833121266546, 20.69640364028325052, -1.500000000000002220 ) ) ;
#55943=CARTESIAN_POINT ( 'NONE',  ( -1.126084586642228436, -21.63456646517454729, 11.49999999999999645 ) ) ;
#55947=CARTESIAN_POINT ( 'NONE',  ( 5.309366582633749054, -21.77581755331916824, 11.49999999999998934 ) ) ;
#55948=FACE_OUTER_BOUND ( 'NONE', #76985, .T. ) ;
#55952=CARTESIAN_POINT ( 'NONE',  ( -35.47953491189426956, -24.63419186844611630, 9.035850630976925757 ) ) ;
#55954=EDGE_LOOP ( 'NONE', ( #81488, #92514, #89062, #13112 ) ) ;
#55956=PLANE ( 'NONE',  #50655 ) ;
#55957=VERTEX_POINT ( 'NONE', #17559 ) ;
#55959=ADVANCED_FACE ( 'NONE', ( #42424 ), #11445, .F. ) ;
#55960=CARTESIAN_POINT ( 'NONE',  ( -1.563627757057377110, -21.15500258984412696, -1.500000000000002220 ) ) ;
#55961=ORIENTED_EDGE ( 'NONE', *, *, #56225, .T. ) ;
#55962=CARTESIAN_POINT ( 'NONE',  ( -50.51069548810792753, -23.85016227208580020, -0.8807180028928345283 ) ) ;
#55963=ADVANCED_FACE ( 'NONE', ( #96678 ), #27179, .F. ) ;
#55964=B_SPLINE_CURVE_WITH_KNOTS ( 'NONE', 3,
 ( #57012, #87949, #80328, #3232, #1714, #34165, #47889, #32650 ),
 .UNSPECIFIED., .F., .F.,
 ( 4, 2, 2, 4 ),
 ( 6.391158118975384497E-06, 0.002007136338672933090, 0.003007508928949907765, 0.004007881519226881573 ),
 .UNSPECIFIED. ) ;
#55965=CARTESIAN_POINT ( 'NONE',  ( 8.287826148123016878, -20.17477452812186201, 11.49999999999998934 ) ) ;
#55966=CARTESIAN_POINT ( 'NONE',  ( -103.6267837749912957, -24.35071581493543391, 9.817618358456027039 ) ) ;
#55967=EDGE_CURVE ( 'NONE', #13730, #85108, #68935, .T. ) ;
#55968=CARTESIAN_POINT ( 'NONE',  ( -62.58953762381672448, -24.66019654487198665, 8.947790411086129936 ) ) ;
#55969=CARTESIAN_POINT ( 'NONE',  ( -35.52287095715008292, -23.84081130425356676, 10.88220057483159309 ) ) ;
#55970=CARTESIAN_POINT ( 'NONE',  ( 4.989390281198801347, -21.28523531580253803, -1.500000000000002220 ) ) ;
#55972=ORIENTED_EDGE ( 'NONE', *, *, #44864, .T. ) ;
#55973=CARTESIAN_POINT ( 'NONE',  ( -40.43756433397305017, -25.12049752546737835, 2.832404795212222659 ) ) ;
#55974=CARTESIAN_POINT ( 'NONE',  ( -85.65008588651460286, -23.48786465467240703, 11.44779295918254647 ) ) ;
#55975=ORIENTED_EDGE ( 'NONE', *, *, #64015, .F. ) ;
#55977=ADVANCED_FACE ( 'NONE', ( #35297 ), #98165, .T. ) ;
#55978=EDGE_CURVE ( 'NONE', #79255, #86407, #67246, .T. ) ;
#55981=EDGE_CURVE ( 'NONE', #55313, #70518, #27781, .T. ) ;
#55985=CARTESIAN_POINT ( 'NONE',  ( -31.24388727629349560, -25.13054166897875774, 2.818273575189820690 ) ) ;
#55986=CARTESIAN_POINT ( 'NONE',  ( 15.87343765641381665, 14.11872912734625274, 11.49999999999998934 ) ) ;
#55987=CARTESIAN_POINT ( 'NONE',  ( -122.5228709571500616, -24.64965694238408034, 8.947790433994191162 ) ) ;
#55988=CARTESIAN_POINT ( 'NONE',  ( -130.5728709571501156, -25.57033040079278763, 6.142048374048878046 ) ) ;
#55989=DIRECTION ( 'NONE',  ( 0.000000000000000000, -0.9999999999976377785, -2.173523156925979128E-06 ) ) ;
#55991=CARTESIAN_POINT ( 'NONE',  ( 12.39309347844599252, 14.90900669795185252, 11.49999999999998934 ) ) ;
#55992=CARTESIAN_POINT ( 'NONE',  ( -117.6235066768902016, -24.66019654487200441, 8.947790411086110396 ) ) ;
#55994=CARTESIAN_POINT ( 'NONE',  ( 19.46547125265945155, -1.073068822128883104, 11.49999999999999645 ) ) ;
#55997=EDGE_CURVE ( 'NONE', #53720, #22015, #35162, .T. ) ;
#55998=ORIENTED_EDGE ( 'NONE', *, *, #80542, .T. ) ;
#56001=CARTESIAN_POINT ( 'NONE',  ( -51.52287095715009002, -23.48783264082477018, -1.443836473390092578 ) ) ;
#56002=CARTESIAN_POINT ( 'NONE',  ( -81.87824661256287584, -25.24813725404296960, 6.339755482797981401 ) ) ;
#56003=CARTESIAN_POINT ( 'NONE',  ( -17.62174901100306101, -8.731699659924187173, 11.49999999999998934 ) ) ;
#56005=ORIENTED_EDGE ( 'NONE', *, *, #87511, .T. ) ;
#56007=LINE ( 'NONE', #86932, #99063 ) ;
#56008=CARTESIAN_POINT ( 'NONE',  ( -22.63574357292403860, -4.499050354539342322, -1.500000000000002220 ) ) ;
#56010=CARTESIAN_POINT ( 'NONE',  ( -106.5895376238167529, -24.64965694238407679, 8.947790433994649462 ) ) ;
#56012=CARTESIAN_POINT ( 'NONE',  ( -97.62752127768544597, -24.35071581493544102, 9.817618358456025263 ) ) ;
#56015=CARTESIAN_POINT ( 'NONE',  ( -129.5217893627370245, -24.65952944569305316, 1.056160979905705899 ) ) ;
#56016=CARTESIAN_POINT ( 'NONE',  ( -99.12822588951706848, -25.31565927954684625, 4.142262207320525746 ) ) ;
#56017=CARTESIAN_POINT ( 'NONE',  ( -19.52388446859773552, -3.948942086532154061, -1.500000000000002220 ) ) ;
#56018=CARTESIAN_POINT ( 'NONE',  ( -68.52287095715006160, -23.48786465467241058, 11.44779295918254647 ) ) ;
#56019=CARTESIAN_POINT ( 'NONE',  ( -4.105667982141768313, -19.37954422259287668, -1.500000000000002220 ) ) ;
#56023=B_SPLINE_CURVE_WITH_KNOTS ( 'NONE', 3,
 ( #3331, #33249, #80931, #58113, #64229, #25640 ),
 .UNSPECIFIED., .F., .F.,
 ( 4, 2, 4 ),
 ( 0.000000000000000000, 0.001380901958385395700, 0.002761803916770791401 ),
 .UNSPECIFIED. ) ;
#56025=DIRECTION ( 'NONE',  ( -0.000000000000000000, 2.173523156925979552E-06, -0.9999999999976378895 ) ) ;
#56026=CARTESIAN_POINT ( 'NONE',  ( -14.56105648253378781, -14.73650127990469016, 11.49999999999999645 ) ) ;
#56029=CARTESIAN_POINT ( 'NONE',  ( -126.5895376238167529, -24.64898659630529565, 1.056161002820836359 ) ) ;
#56030=CARTESIAN_POINT ( 'NONE',  ( 22.20067557195093855, 5.203973054738295190, 11.49999999999999645 ) ) ;
#56033=CARTESIAN_POINT ( 'NONE',  ( -69.50623498437037995, -24.15543982623907482, -0.2315651400026648155 ) ) ;
#56034=CARTESIAN_POINT ( 'NONE',  ( -89.58953762381671027, -23.47596703998600631, 11.44779298504227683 ) ) ;
#56037=CARTESIAN_POINT ( 'NONE',  ( 11.17094659993960803, -16.83544227557131023, -1.500000000000002220 ) ) ;
#56038=CARTESIAN_POINT ( 'NONE',  ( -89.92287095715005307, -23.47596703998600631, 11.44779298504227860 ) ) ;
#56040=CARTESIAN_POINT ( 'NONE',  ( -41.22892028381910734, -25.30353790740849007, 4.765619386710907790 ) ) ;
#56044=CARTESIAN_POINT ( 'NONE',  ( -84.52287095715006160, -23.47596703998600631, 11.44779298504228571 ) ) ;
#56045=CARTESIAN_POINT ( 'NONE',  ( -18.22994410263883225, 8.285605901428201747, -1.500000000000002220 ) ) ;
#56046=CARTESIAN_POINT ( 'NONE',  ( -110.3139465455115129, -25.11033443737754212, 2.832404817301930056 ) ) ;
#56047=CARTESIAN_POINT ( 'NONE',  ( 18.03207908435136986, 10.65457695745678457, 11.49999999999999645 ) ) ;
#56048=CARTESIAN_POINT ( 'NONE',  ( -54.62287095715005592, -23.48786465467240347, 11.44779295918255180 ) ) ;
#56050=CARTESIAN_POINT ( 'NONE',  ( 20.57837473233041692, -7.934362236255416256, -1.500000000000002220 ) ) ;
#56055=DIRECTION ( 'NONE',  ( 1.000000000000000000, 3.773278334444166432E-23, 8.201307841325785021E-29 ) ) ;
#56058=ORIENTED_EDGE ( 'NONE', *, *, #56796, .T. ) ;
#56059=ORIENTED_EDGE ( 'NONE', *, *, #4977, .F. ) ;
#56060=CARTESIAN_POINT ( 'NONE',  ( -78.62287095715005592, -23.47593901973091235, -1.443836447539004642 ) ) ;
#56062=CARTESIAN_POINT ( 'NONE',  ( -96.62287095715005592, -29.50250786944525672, 11.44777988621623166 ) ) ;
#56063=CARTESIAN_POINT ( 'NONE',  ( -19.72667040167412722, -5.651925516699977337, -1.500000000000002220 ) ) ;
#56064=VERTEX_POINT ( 'NONE', #53017 ) ;
#56065=CARTESIAN_POINT ( 'NONE',  ( -116.6228709571500417, -24.66019654487199730, 8.947790411086121054 ) ) ;
#56068=CARTESIAN_POINT ( 'NONE',  ( 21.15698459081360383, -7.064864530413820454, 11.49999999999998934 ) ) ;
#56069=DIRECTION ( 'NONE',  ( -3.773278334453079618E-23, 0.9999999999976377785, 2.173523156925979975E-06 ) ) ;
#56070=CARTESIAN_POINT ( 'NONE',  ( -125.6228709571500559, -23.48786465467241769, 11.44779295918253403 ) ) ;
#56074=CARTESIAN_POINT ( 'NONE',  ( 4.135342931496230001, -20.44547621892628797, 11.49999999999998934 ) ) ;
#56079=ADVANCED_FACE ( 'NONE', ( #36783 ), #66759, .T. ) ;
#56081=CARTESIAN_POINT ( 'NONE',  ( -1.999300432013352058, 20.99099883833691749, -1.500000000000002220 ) ) ;
#56082=ORIENTED_EDGE ( 'NONE', *, *, #99474, .T. ) ;
#56086=CARTESIAN_POINT ( 'NONE',  ( -120.5922445377380114, -23.85049219812686871, 10.88485053497526778 ) ) ;
#56087=CARTESIAN_POINT ( 'NONE',  ( -86.55452498666917904, -23.96169478059713498, 10.65365249895717881 ) ) ;
#56088=CARTESIAN_POINT ( 'NONE',  ( -59.54826027102925678, -24.15543982623906416, -0.2315651400026668416 ) ) ;
#56089=CARTESIAN_POINT ( 'NONE',  ( -73.52287095715007581, -29.50248528299804818, 1.056150453629036701 ) ) ;
#56091=CARTESIAN_POINT ( 'NONE',  ( -21.14055147415990277, -6.693858341896442354, 11.49999999999999645 ) ) ;
#56092=EDGE_LOOP ( 'NONE', ( #75387, #52146, #12100, #83375 ) ) ;
#56093=CARTESIAN_POINT ( 'NONE',  ( -99.00614725376551917, -25.30400258354788434, 5.550674214932294959 ) ) ;
#56097=CARTESIAN_POINT ( 'NONE',  ( -21.51096707683950626, -7.176001652309477841, 11.49999999999998934 ) ) ;
#56100=CARTESIAN_POINT ( 'NONE',  ( -76.62287095715007013, -23.47593901973091235, -1.443836447539004642 ) ) ;
#56102=EDGE_CURVE ( 'NONE', #73050, #61311, #15540, .T. ) ;
#56104=ADVANCED_FACE ( 'NONE', ( #16420 ), #51499, .T. ) ;
#56106=AXIS2_PLACEMENT_3D ( 'NONE', #53047, #30689, #61166 ) ;
#56107=CARTESIAN_POINT ( 'NONE',  ( 1.109688723463823301, -20.12803150795971874, 11.49999999999998934 ) ) ;
#56112=CARTESIAN_POINT ( 'NONE',  ( -18.94483701893047467, 11.91932228829616669, -1.500000000000002220 ) ) ;
#56113=VECTOR ( 'NONE', #46257, 1000.000000000000114 ) ;
#56114=B_SPLINE_CURVE_WITH_KNOTS ( 'NONE', 3,
 ( #30927, #53279, #77589, #91824 ),
 .UNSPECIFIED., .F., .F.,
 ( 4, 4 ),
 ( 0.000000000000000000, 1.000000000000000000 ),
 .UNSPECIFIED. ) ;
#56115=VECTOR ( 'NONE', #1586, 1000.000000000000114 ) ;
#56116=VERTEX_POINT ( 'NONE', #30662 ) ;
#56117=ORIENTED_EDGE ( 'NONE', *, *, #97955, .F. ) ;
#56118=CARTESIAN_POINT ( 'NONE',  ( -112.5918939201014553, -23.96169478059713498, 10.65365249895717348 ) ) ;
#56120=CARTESIAN_POINT ( 'NONE',  ( -39.49513710205338413, -25.30491637845361552, 4.489908266797987935 ) ) ;
#56124=CARTESIAN_POINT ( 'NONE',  ( -5.392953615240748455, 18.82278424538476713, -1.500000000000002220 ) ) ;
#56125=CARTESIAN_POINT ( 'NONE',  ( -46.56050886298546487, -23.73766607897669800, -1.055555164236460230 ) ) ;
#56127=CARTESIAN_POINT ( 'NONE',  ( 8.900169022907615357, -19.58186849131130813, 11.49999999999998934 ) ) ;
#56128=CARTESIAN_POINT ( 'NONE',  ( -128.5217325982747241, -24.15543982623908548, -0.2315651400026392803 ) ) ;
#56130=CARTESIAN_POINT ( 'NONE',  ( -101.5391830360295558, -25.20975163562174259, 3.394848129468846842 ) ) ;
#56132=CARTESIAN_POINT ( 'NONE',  ( -9.034649315346676701, 21.08484869742704504, -1.500000000000002220 ) ) ;
#56134=CARTESIAN_POINT ( 'NONE',  ( -71.30261592386577263, -25.26164592712893509, 6.148532042880709980 ) ) ;
#56135=CARTESIAN_POINT ( 'NONE',  ( -16.75416981316412190, 10.96944243606782443, 11.49999999999999645 ) ) ;
#56137=CARTESIAN_POINT ( 'NONE',  ( -76.62287095715007013, -29.50250786944525672, 11.44777988621623521 ) ) ;
#56138=LINE ( 'NONE', #41403, #57156 ) ;
#56140=CARTESIAN_POINT ( 'NONE',  ( -50.62287095715007013, -24.15516710230294350, 10.28746687063725673 ) ) ;
#56141=CARTESIAN_POINT ( 'NONE',  ( -19.53060160647804722, 3.385818350044136338, 11.49999999999998934 ) ) ;
#56142=CARTESIAN_POINT ( 'NONE',  ( 20.57166443188586769, -7.073620337204646447, 11.49999999999998934 ) ) ;
#56143=CARTESIAN_POINT ( 'NONE',  ( -107.6228709571500701, -29.50248528299804818, 1.056150453629043584 ) ) ;
#56144=CARTESIAN_POINT ( 'NONE',  ( -9.385407830382300531, 17.29636241635495608, -1.500000000000002220 ) ) ;
#56146=CARTESIAN_POINT ( 'NONE',  ( -42.60798218881454602, -23.73766607897670156, -1.055555164236442689 ) ) ;
#56147=CARTESIAN_POINT ( 'NONE',  ( -41.62287095715006302, -23.48786465467240703, 11.44779295918255180 ) ) ;
#56149=CARTESIAN_POINT ( 'NONE',  ( -115.6228709571500275, -23.84047902841603772, -0.8780736468305494480 ) ) ;
#56151=CARTESIAN_POINT ( 'NONE',  ( 17.26003113218828489, 11.23261964116016642, 11.49999999999999645 ) ) ;
#56152=DIRECTION ( 'NONE',  ( 0.000000000000000000, 0.9999999999976377785, 2.173523156925979975E-06 ) ) ;
#56154=CARTESIAN_POINT ( 'NONE',  ( -120.6258288809107029, -24.40034930558991633, 0.3402023900116107336 ) ) ;
#56155=CARTESIAN_POINT ( 'NONE',  ( -7.157701736792966507, -21.45640540170154509, 11.49999999999999645 ) ) ;
#56157=EDGE_CURVE ( 'NONE', #56235, #66681, #17432, .T. ) ;
#56158=CARTESIAN_POINT ( 'NONE',  ( -100.3574794290996266, -25.31296445282071161, 4.711073526889959062 ) ) ;
#56160=CARTESIAN_POINT ( 'NONE',  ( -97.62356136723437317, -24.65952944569304961, 1.056160979905703456 ) ) ;
#56161=CARTESIAN_POINT ( 'NONE',  ( -27.40053816590288704, -24.76668234067835783, 2.305505410589911985 ) ) ;
#56163=B_SPLINE_CURVE_WITH_KNOTS ( 'NONE', 3,
 ( #52251, #83178, #73590, #50257, #13662, #11673 ),
 .UNSPECIFIED., .F., .F.,
 ( 4, 2, 4 ),
 ( 1.570755371634013412E-05, 0.001396183895866086669, 0.002776660238015832977 ),
 .UNSPECIFIED. ) ;
#56164=CARTESIAN_POINT ( 'NONE',  ( -125.6228709571500559, -23.47596703998600631, 11.44779298504227860 ) ) ;
#56166=EDGE_LOOP ( 'NONE', ( #33999, #47352, #3792, #99570 ) ) ;
#56167=CARTESIAN_POINT ( 'NONE',  ( -79.41916052885848387, -25.31596350975968335, 5.559759362272460592 ) ) ;
#56168=CARTESIAN_POINT ( 'NONE',  ( -2.521034868938843765, 22.70145277337256218, -1.500000000000002220 ) ) ;
#56171=CARTESIAN_POINT ( 'NONE',  ( -82.58824230787639920, -24.35071581493543036, 9.817618358456032368 ) ) ;
#56172=CARTESIAN_POINT ( 'NONE',  ( -11.50411854321151672, 19.32100693743031528, 11.49999999999999645 ) ) ;
#56175=CARTESIAN_POINT ( 'NONE',  ( -16.59477544326466969, -14.39948450415919723, 11.49999999999998934 ) ) ;
#56176=B_SPLINE_CURVE_WITH_KNOTS ( 'NONE', 3,
 ( #38846, #37366, #67824, #100220 ),
 .UNSPECIFIED., .F., .F.,
 ( 4, 4 ),
 ( 0.000000000000000000, 9.999999999998897304E-05 ),
 .UNSPECIFIED. ) ;
#56177=EDGE_CURVE ( 'NONE', #65451, #90447, #81716, .T. ) ;
#56178=CARTESIAN_POINT ( 'NONE',  ( -114.5228709571500332, -24.50321055353804667, 9.387540953477513384 ) ) ;
#56180=CARTESIAN_POINT ( 'NONE',  ( -44.54660971391017199, -24.15620529776628089, 10.23563542870660470 ) ) ;
#56181=CARTESIAN_POINT ( 'NONE',  ( -68.97952899265784765, -25.20747150332676867, 6.546521981683093294 ) ) ;
#56183=CARTESIAN_POINT ( 'NONE',  ( -48.58718991420165878, -24.35071581493542681, 9.817618358456027039 ) ) ;
#56187=CARTESIAN_POINT ( 'NONE',  ( 20.39306652673287701, -2.074774109220689500, 11.49999999999998934 ) ) ;
#56193=CARTESIAN_POINT ( 'NONE',  ( 21.72910700495702230, 7.846448622349001312, 11.49999999999998934 ) ) ;
#56195=CARTESIAN_POINT ( 'NONE',  ( 20.34676669208793953, -0.1217515720461415790, -1.500000000000002220 ) ) ;
#56197=CARTESIAN_POINT ( 'NONE',  ( -84.52287095715006160, -29.50250243563736774, 8.947779886222141599 ) ) ;
#56198=CARTESIAN_POINT ( 'NONE',  ( -92.51227642707885934, -24.15543982623908192, -0.2315651400026453588 ) ) ;
#56202=CARTESIAN_POINT ( 'NONE',  ( -10.19830463584622571, -18.94658877215714909, 11.49999999999999645 ) ) ;
#56203=EDGE_LOOP ( 'NONE', ( #97386, #35603, #18502, #19076 ) ) ;
#56204=CARTESIAN_POINT ( 'NONE',  ( -75.54003180113411986, -24.73486907724918282, 1.287355809206967683 ) ) ;
#56205=CARTESIAN_POINT ( 'NONE',  ( -49.59506520832605503, -25.26385825920966610, 4.856709818570129400 ) ) ;
#56206=ORIENTED_EDGE ( 'NONE', *, *, #71322, .T. ) ;
#56207=CARTESIAN_POINT ( 'NONE',  ( -10.32638548400381673, 17.97674989526738898, -1.500000000000002220 ) ) ;
#56208=ORIENTED_EDGE ( 'NONE', *, *, #49467, .F. ) ;
#56209=CARTESIAN_POINT ( 'NONE',  ( -125.5556659931842347, -24.15503026093915295, -0.2815557561904348804 ) ) ;
#56210=EDGE_LOOP ( 'NONE', ( #61453, #53426, #3982, #18379 ) ) ;
#56212=CARTESIAN_POINT ( 'NONE',  ( -48.52287095715004739, -24.51283580621457858, 0.6167428607047514832 ) ) ;
#56216=DIRECTION ( 'NONE',  ( 0.000000000000000000, -2.173523156925979552E-06, 0.9999999999976378895 ) ) ;
#56218=CARTESIAN_POINT ( 'NONE',  ( -18.71521858236628333, -11.60751834597489740, 11.49999999999999645 ) ) ;
#56219=VERTEX_POINT ( 'NONE', #59380 ) ;
#56220=CARTESIAN_POINT ( 'NONE',  ( -103.5871832607983976, -24.51314013834315375, 0.6176544820404142877 ) ) ;
#56221=ADVANCED_FACE ( 'NONE', ( #47895 ), #33155, .T. ) ;
#56222=CARTESIAN_POINT ( 'NONE',  ( -22.56969522194696509, -0.6267768857631424995, 11.49999999999998934 ) ) ;
#56224=CARTESIAN_POINT ( 'NONE',  ( 16.30764028314251846, 13.22082560946828522, 11.49999999999998934 ) ) ;
#56225=EDGE_CURVE ( 'NONE', #25080, #65405, #76102, .T. ) ;
#56227=ORIENTED_EDGE ( 'NONE', *, *, #6473, .F. ) ;
#56228=B_SPLINE_CURVE_WITH_KNOTS ( 'NONE', 3,
 ( #64976, #49739, #64479, #50724 ),
 .UNSPECIFIED., .F., .F.,
 ( 4, 4 ),
 ( 0.000000000000000000, 1.000000000000000000 ),
 .UNSPECIFIED. ) ;
#56230=VERTEX_POINT ( 'NONE', #71732 ) ;
#56232=EDGE_CURVE ( 'NONE', #88005, #79117, #13201, .T. ) ;
#56233=PLANE ( 'NONE',  #67728 ) ;
#56234=DIRECTION ( 'NONE',  ( -3.773278334453080206E-23, 0.9999999999976377785, 2.173523156925979975E-06 ) ) ;
#56235=VERTEX_POINT ( 'NONE', #12690 ) ;
#56236=CARTESIAN_POINT ( 'NONE',  ( 13.25904570721172604, 16.46799385432867169, 11.49999999999998934 ) ) ;
#56237=CARTESIAN_POINT ( 'NONE',  ( -66.62287095715005592, -24.64965695001468404, 8.947790433994184056 ) ) ;
#56238=CARTESIAN_POINT ( 'NONE',  ( -51.83680534327738343, -25.03148548991196520, 6.675008763280794177 ) ) ;
#56239=CARTESIAN_POINT ( 'NONE',  ( -75.62287095715004170, -24.91544648472620693, 1.928969306349227919 ) ) ;
#56242=CARTESIAN_POINT ( 'NONE',  ( 19.92104321119709098, 9.795001720801039369, -1.500000000000002220 ) ) ;
#56243=CARTESIAN_POINT ( 'NONE',  ( -114.6235148628036882, -24.65952944569305316, 1.056160979905706343 ) ) ;
#56246=CARTESIAN_POINT ( 'NONE',  ( -112.5228709571501184, -24.34917612407046761, 0.1852690917481127075 ) ) ;
#56248=CARTESIAN_POINT ( 'NONE',  ( -8.724563080612403709, -17.33930400145671413, 11.49999999999999645 ) ) ;
#56249=DIRECTION ( 'NONE',  ( -1.000000000000000000, -3.773278334444166432E-23, -8.201307841325785021E-29 ) ) ;
#56251=B_SPLINE_CURVE_WITH_KNOTS ( 'NONE', 3,
 ( #80552, #65362, #42511, #95283, #97278, #3450, #25768, #96776, #73449, #35391, #56740, #58231, #3942, #27275, #89170, #19643 ),
 .UNSPECIFIED., .F., .F.,
 ( 4, 2, 2, 2, 2, 2, 2, 4 ),
 ( 0.000000000000000000, 0.0002653022231966347061, 0.0005306044463932694123, 0.001061208892786539692, 0.001326511115983166483, 0.001591813339179793492, 0.001857115562376420283, 0.002122417785573047291 ),
 .UNSPECIFIED. ) ;
#56252=CARTESIAN_POINT ( 'NONE',  ( -18.70048401425367501, 5.426029767813830063, 11.49999999999998934 ) ) ;
#56253=CARTESIAN_POINT ( 'NONE',  ( 21.39645853268639186, 0.3907444525687319703, -1.500000000000002220 ) ) ;
#56255=CARTESIAN_POINT ( 'NONE',  ( -60.49376913606877793, -24.52399227489757649, 9.353111116819363247 ) ) ;
#56256=CARTESIAN_POINT ( 'NONE',  ( -51.51436549635971573, -23.73766607897669445, -1.055555164236457788 ) ) ;
#56257=FACE_OUTER_BOUND ( 'NONE', #43740, .T. ) ;
#56258=CARTESIAN_POINT ( 'NONE',  ( 10.97283692364161922, -19.94330716608196852, -1.500000000000002220 ) ) ;
#56261=CARTESIAN_POINT ( 'NONE',  ( -106.5874605220203364, -24.51419770103158768, 9.386484678747164523 ) ) ;
#56263=CARTESIAN_POINT ( 'NONE',  ( -16.51628311069853083, -11.03946451426814690, 11.49999999999999645 ) ) ;
#56265=VECTOR ( 'NONE', #16376, 1000.000000000000114 ) ;
#56266=DIRECTION ( 'NONE',  ( 0.000000000000000000, 2.173523156925980399E-06, -0.9999999999976378895 ) ) ;
#56267=B_SPLINE_CURVE_WITH_KNOTS ( 'NONE', 3,
 ( #59628, #74830, #90560, #14425 ),
 .UNSPECIFIED., .F., .F.,
 ( 4, 4 ),
 ( 0.4000716058185329049, 0.4090780370906481611 ),
 .UNSPECIFIED. ) ;
#56269=VERTEX_POINT ( 'NONE', #83195 ) ;
#56270=CARTESIAN_POINT ( 'NONE',  ( -49.74068094892759007, -25.14920433696932633, 6.948203997227099471 ) ) ;
#56272=CARTESIAN_POINT ( 'NONE',  ( -51.66021737866784491, -25.27412416137573459, 3.699308556398079428 ) ) ;
#56273=CARTESIAN_POINT ( 'NONE',  ( -6.031157642910047301, -20.80930661755759203, -1.500000000000002220 ) ) ;
#56274=CARTESIAN_POINT ( 'NONE',  ( -50.50587993032255696, -25.04358547397666968, 7.560798279822890322 ) ) ;
#56275=CARTESIAN_POINT ( 'NONE',  ( -3.338044803349280443, -19.22079736023769669, -1.500000000000002220 ) ) ;
#56276=CARTESIAN_POINT ( 'NONE',  ( -123.6228709571500417, -23.73934037231757799, 11.05740245334328264 ) ) ;
#56277=EDGE_CURVE ( 'NONE', #56961, #85635, #34971, .T. ) ;
#56278=ORIENTED_EDGE ( 'NONE', *, *, #84868, .F. ) ;
#56279=CARTESIAN_POINT ( 'NONE',  ( -8.611577853089924517, -18.50786853157798006, 11.49999999999999645 ) ) ;
#56281=EDGE_CURVE ( 'NONE', #49859, #5012, #7581, .T. ) ;
#56282=CARTESIAN_POINT ( 'NONE',  ( -41.62287095715006302, -23.47593901973091235, -1.443836447539011525 ) ) ;
#56286=CARTESIAN_POINT ( 'NONE',  ( -39.04454818115137016, -25.27985276553044969, 4.262458935199855858 ) ) ;
#56287=CARTESIAN_POINT ( 'NONE',  ( -49.40320226356282518, -25.25138784447102225, 5.711994385046795131 ) ) ;
#56288=CARTESIAN_POINT ( 'NONE',  ( -86.52287095715001897, -24.51283580621457148, 0.6167428607047598099 ) ) ;
#56289=B_SPLINE_CURVE_WITH_KNOTS ( 'NONE', 3,
 ( #83073, #21669, #15072, #46040, #74964, #30292 ),
 .UNSPECIFIED., .F., .F.,
 ( 4, 2, 4 ),
 ( 0.000000000000000000, 0.001380901958385387894, 0.002761803916770775788 ),
 .UNSPECIFIED. ) ;
#56290=CARTESIAN_POINT ( 'NONE',  ( -89.58953762381671027, -24.66019654487199730, 8.947790411086124607 ) ) ;
#56291=EDGE_LOOP ( 'NONE', ( #84387, #67918, #83121, #35281 ) ) ;
#56292=CARTESIAN_POINT ( 'NONE',  ( -42.62287095715004881, -24.65952944569303895, 1.056160979905691688 ) ) ;
#56294=CARTESIAN_POINT ( 'NONE',  ( -1.334576548209915225, -22.92891363262047832, 11.49999999999999645 ) ) ;
#56295=CARTESIAN_POINT ( 'NONE',  ( 18.51665531608540860, 13.21585733361752801, 11.49999999999998934 ) ) ;
#56296=EDGE_LOOP ( 'NONE', ( #80004, #55156, #64931, #89745 ) ) ;
#56299=CARTESIAN_POINT ( 'NONE',  ( -75.62287095715005592, -24.52323809116984776, 9.355190652339420154 ) ) ;
#56300=CARTESIAN_POINT ( 'NONE',  ( -123.5228709571501184, -24.66019654487200441, 8.947790411086105067 ) ) ;
#56302=CARTESIAN_POINT ( 'NONE',  ( -30.57287095715006231, -25.26620738237330954, 3.875798415478208359 ) ) ;
#56305=CARTESIAN_POINT ( 'NONE',  ( -26.99091393574990150, -24.76286136825473250, 2.476735171210982411 ) ) ;
#56306=CARTESIAN_POINT ( 'NONE',  ( -76.92287095715005307, -23.47596703998600631, 11.44779298504227860 ) ) ;
#56307=CARTESIAN_POINT ( 'NONE',  ( -34.58953762381672448, -24.65952944569304250, 1.056160979905690134 ) ) ;
#56310=CARTESIAN_POINT ( 'NONE',  ( -10.90597124047809530, 17.21661415904998904, 11.49999999999998934 ) ) ;
#56311=VERTEX_POINT ( 'NONE', #13683 ) ;
#56312=ORIENTED_EDGE ( 'NONE', *, *, #37587, .F. ) ;
#56313=CARTESIAN_POINT ( 'NONE',  ( -22.55714481399219906, -4.634528848986672500, 11.49999999999998934 ) ) ;
#56316=ORIENTED_EDGE ( 'NONE', *, *, #78278, .F. ) ;
#56318=CARTESIAN_POINT ( 'NONE',  ( -32.52287095715004739, -24.34917612407030774, 0.1852690917476929044 ) ) ;
#56319=CARTESIAN_POINT ( 'NONE',  ( -95.59440297368489325, -24.15503026093913874, -0.2815557561904519224 ) ) ;
#56321=CARTESIAN_POINT ( 'NONE',  ( -14.93283513470682067, -15.21490397768744529, 11.49999999999999645 ) ) ;
#56324=CARTESIAN_POINT ( 'NONE',  ( -19.85906585229243504, 9.992431322412627992, 11.49999999999998934 ) ) ;
#56325=CARTESIAN_POINT ( 'NONE',  ( 20.50092990308456464, -2.467789585553555654, 11.49999999999998934 ) ) ;
#56327=ORIENTED_EDGE ( 'NONE', *, *, #70427, .T. ) ;
#56328=CARTESIAN_POINT ( 'NONE',  ( -125.5228709571500616, -29.50248528299804818, 1.056150453629047137 ) ) ;
#56329=CARTESIAN_POINT ( 'NONE',  ( -71.72497398431139004, -25.25978459231412288, 3.590539514744167437 ) ) ;
#56330=ORIENTED_EDGE ( 'NONE', *, *, #19760, .T. ) ;
#56331=CARTESIAN_POINT ( 'NONE',  ( -95.52287095715004739, -23.84047902841604127, -0.8780736468305392339 ) ) ;
#56332=VECTOR ( 'NONE', #24377, 1000.000000000000114 ) ;
#56333=ORIENTED_EDGE ( 'NONE', *, *, #26175, .F. ) ;
#56334=CARTESIAN_POINT ( 'NONE',  ( -58.59294932955677382, -24.15620529776628089, 10.23563542870660470 ) ) ;
#56336=CARTESIAN_POINT ( 'NONE',  ( -20.82246440549779720, 1.468558417816581807, -1.500000000000002220 ) ) ;
#56338=CARTESIAN_POINT ( 'NONE',  ( 19.20967809413044236, -10.42350525531561978, 11.49999999999999645 ) ) ;
#56339=CARTESIAN_POINT ( 'NONE',  ( -37.52287095715006870, -24.64898659630367206, 1.056161002820819261 ) ) ;
#56341=CARTESIAN_POINT ( 'NONE',  ( -18.88510386880526326, 12.19974334031638641, 11.49999999999998934 ) ) ;
#56342=CARTESIAN_POINT ( 'NONE',  ( -38.59385446322277602, -24.15543982623906771, -0.2315651400026570161 ) ) ;
#56345=ORIENTED_EDGE ( 'NONE', *, *, #9303, .T. ) ;
#56346=ADVANCED_FACE ( 'NONE', ( #68981 ), #75087, .F. ) ;
#56347=ORIENTED_EDGE ( 'NONE', *, *, #62216, .F. ) ;
#56348=ORIENTED_EDGE ( 'NONE', *, *, #50464, .T. ) ;
#56350=CARTESIAN_POINT ( 'NONE',  ( -52.63306204174769221, -24.34968618360933945, 0.1864209137778880532 ) ) ;
#56351=VERTEX_POINT ( 'NONE', #76083 ) ;
#56352=CARTESIAN_POINT ( 'NONE',  ( 18.99370601119529312, 9.851043883551550806, -1.500000000000002220 ) ) ;
#56353=CARTESIAN_POINT ( 'NONE',  ( -16.90645664988545249, 14.66980924573920397, 11.49999999999999645 ) ) ;
#56354=ORIENTED_EDGE ( 'NONE', *, *, #48087, .F. ) ;
#56355=CARTESIAN_POINT ( 'NONE',  ( -68.52287095715006160, -24.65952944569304606, 1.056160979905697239 ) ) ;
#56356=CARTESIAN_POINT ( 'NONE',  ( -20.60145385712877797, -4.430719527714695793, -1.500000000000002220 ) ) ;
#56357=CARTESIAN_POINT ( 'NONE',  ( -30.58829336780489072, -23.48332523652080539, 11.44779287168131710 ) ) ;
#56358=CARTESIAN_POINT ( 'NONE',  ( 14.81759351585047391, 13.34335055255382052, -1.500000000000002220 ) ) ;
#56360=CARTESIAN_POINT ( 'NONE',  ( -113.6228709571500559, -23.47593901973091235, -1.443836447538999312 ) ) ;
#56361=CARTESIAN_POINT ( 'NONE',  ( -101.5528341795800316, -24.15543982623907482, -0.2315651400026588758 ) ) ;
#56362=CARTESIAN_POINT ( 'NONE',  ( -20.26759042640731323, -8.618136523154847239, -1.500000000000002220 ) ) ;
#56363=ORIENTED_EDGE ( 'NONE', *, *, #83668, .F. ) ;
#56364=CARTESIAN_POINT ( 'NONE',  ( -116.5185805412094311, -24.15543982623908548, -0.2315651400026407236 ) ) ;
#56366=DIRECTION ( 'NONE',  ( -3.773278334453079618E-23, 0.9999999999976377785, 2.173523156925979975E-06 ) ) ;
#56367=CARTESIAN_POINT ( 'NONE',  ( -20.64841573231975147, 3.066018724555340746, 11.49999999999999645 ) ) ;
#56368=AXIS2_PLACEMENT_3D ( 'NONE', #1294, #2299, #78891 ) ;
#56369=CARTESIAN_POINT ( 'NONE',  ( -62.49922300485171434, -24.35071581493542681, 9.817618358456032368 ) ) ;
#56370=CARTESIAN_POINT ( 'NONE',  ( -125.5228709571500616, -24.62285846331435835, 9.038163153548284257 ) ) ;
#56371=CARTESIAN_POINT ( 'NONE',  ( -117.5228709571500900, -23.96127896941632685, -0.6493128931037944751 ) ) ;
#56372=CARTESIAN_POINT ( 'NONE',  ( -11.06822068739258391, -18.21809710261049275, -1.500000000000002220 ) ) ;
#56375=CARTESIAN_POINT ( 'NONE',  ( -96.52287095715009002, -23.96177878511310055, 10.65340807706329507 ) ) ;
#56377=CARTESIAN_POINT ( 'NONE',  ( 22.54279463279464579, 0.6884863543687869125, -1.500000000000002220 ) ) ;
#56378=B_SPLINE_SURFACE_WITH_KNOTS ( 'NONE', 3, 1, ( 
 ( #88780, #79646 ),
 ( #94872, #2543 ),
 ( #49726, #12130 ),
 ( #19246, #64966 ),
 ( #73547, #3543 ),
 ( #64468, #56842 ),
 ( #63964, #87774 ),
 ( #18256, #65960 ),
 ( #95877, #81156 ),
 ( #57344, #43102 ),
 ( #74046, #88277 ) ),
 .UNSPECIFIED., .F., .F., .F.,
 ( 4, 1, 1, 1, 1, 1, 1, 1, 4 ),
 ( 2, 2 ),
 ( 0.000000000000000000, 0.1105883385953354281, 0.2245417540535955825, 0.3425034940501039959, 0.4643240984173586106, 0.5907560327017663537, 0.7222274753555145699, 0.8588428362087243695, 1.000000000000000000 ),
 ( 0.000000000000000000, 1.000000000000000000 ),
 .UNSPECIFIED. ) ;
#56379=CARTESIAN_POINT ( 'NONE',  ( -123.5228709571500616, -24.64898659630368627, 1.056161002820833028 ) ) ;
#56380=ORIENTED_EDGE ( 'NONE', *, *, #80360, .T. ) ;
#56382=CARTESIAN_POINT ( 'NONE',  ( -31.61990752757089140, -23.48786465467240347, 11.44779295918255535 ) ) ;
#56383=CARTESIAN_POINT ( 'NONE',  ( -3.718233408413001762, 19.32670252783854536, 11.49999999999999645 ) ) ;
#56384=CARTESIAN_POINT ( 'NONE',  ( -49.52287095715007581, -23.47593901973090169, -1.443836447538997092 ) ) ;
#56386=ORIENTED_EDGE ( 'NONE', *, *, #99154, .T. ) ;
#56387=CARTESIAN_POINT ( 'NONE',  ( -89.52287095715000476, -24.33927499327855060, 9.819080762295811837 ) ) ;
#56388=CARTESIAN_POINT ( 'NONE',  ( -55.62287095715002749, -24.51163499207175533, 0.6490370598554264792 ) ) ;
#56389=CARTESIAN_POINT ( 'NONE',  ( -124.6242025155618478, -24.35071581493544457, 9.817618358456016381 ) ) ;
#56393=CARTESIAN_POINT ( 'NONE',  ( -48.62287095715004881, -29.50250243563736774, 8.947779886222146928 ) ) ;
#56394=CARTESIAN_POINT ( 'NONE',  ( 8.221391366598689743, 17.94232518691122635, -1.500000000000002220 ) ) ;
#56396=B_SPLINE_CURVE_WITH_KNOTS ( 'NONE', 3,
 ( #4246, #41821, #28081, #4743, #74734, #98064, #67156, #97086, #3261, #89476, #80868, #18959, #96583, #73748, #28571, #5234, #59531, #72766 ),
 .UNSPECIFIED., .F., .F.,
 ( 4, 2, 2, 2, 2, 2, 2, 2, 4 ),
 ( 0.000000000000000000, 0.0002842996626774647244, 0.0005685993253549294487, 0.0008528989880323941189, 0.001137198650709858897, 0.001421498313387323676, 0.001705797976064788238, 0.001990097638742253233, 0.002274397301419717795 ),
 .UNSPECIFIED. ) ;
#56397=CARTESIAN_POINT ( 'NONE',  ( -5.512817753899047268, 19.46650688538001361, 11.49999999999999645 ) ) ;
#56402=CARTESIAN_POINT ( 'NONE',  ( -115.6228709571500559, -23.48786465467242479, 11.44779295918253759 ) ) ;
#56403=CARTESIAN_POINT ( 'NONE',  ( -72.58953762381672448, -23.47596703998600276, 11.44779298504227683 ) ) ;
#56408=CARTESIAN_POINT ( 'NONE',  ( -86.58953762381671027, -24.66019654487199730, 8.947790411086121054 ) ) ;
#56409=CARTESIAN_POINT ( 'NONE',  ( -19.87929632332335927, 2.386914507623989490, 11.49999999999998934 ) ) ;
#56410=LINE ( 'NONE', #78695, #54797 ) ;
#56411=CARTESIAN_POINT ( 'NONE',  ( -87.62287095715004170, -29.50248528299804818, 1.056150453629040253 ) ) ;
#56412=ORIENTED_EDGE ( 'NONE', *, *, #35938, .F. ) ;
#56413=B_SPLINE_CURVE_WITH_KNOTS ( 'NONE', 3,
 ( #95743, #65329, #73415, #58193 ),
 .UNSPECIFIED., .F., .F.,
 ( 4, 4 ),
 ( 0.000000000000000000, 9.999999999998897304E-05 ),
 .UNSPECIFIED. ) ;
#56414=CARTESIAN_POINT ( 'NONE',  ( -79.54656511345403658, -24.35071581493543036, 9.817618358456028815 ) ) ;
#56416=CARTESIAN_POINT ( 'NONE',  ( -100.5228709571500616, -24.99156044556120904, 7.747789690856173195 ) ) ;
#56417=CARTESIAN_POINT ( 'NONE',  ( -116.4728709570019731, -25.40556190190858032, 4.804048521347548117 ) ) ;
#56418=CARTESIAN_POINT ( 'NONE',  ( -73.55905801038284153, -23.73766607897670511, -1.055555164236457344 ) ) ;
#56419=EDGE_CURVE ( 'NONE', #26998, #59330, #8081, .T. ) ;
#56421=CARTESIAN_POINT ( 'NONE',  ( -100.9375798325987716, -25.25978491487772004, 3.590542621692357717 ) ) ;
#56422=ORIENTED_EDGE ( 'NONE', *, *, #18510, .F. ) ;
#56424=CARTESIAN_POINT ( 'NONE',  ( 14.61151973098085222, 14.07909450314327771, -1.500000000000002220 ) ) ;
#56426=CARTESIAN_POINT ( 'NONE',  ( -127.5558934889587448, -23.96169478059714208, 10.65365249895716282 ) ) ;
#56428=CARTESIAN_POINT ( 'NONE',  ( -59.53835329446878433, -24.51419770103156281, 9.386484678747184063 ) ) ;
#56429=ADVANCED_FACE ( 'NONE', ( #24306 ), #54275, .T. ) ;
#56432=CARTESIAN_POINT ( 'NONE',  ( 9.152908845159860363, 19.05633030926415472, 11.49999999999999645 ) ) ;
#56434=CARTESIAN_POINT ( 'NONE',  ( 5.777647480883832287, 21.37485705712154171, -1.500000000000002220 ) ) ;
#56435=CARTESIAN_POINT ( 'NONE',  ( -20.44794078217315558, 2.270689272194197805, -1.500000000000002220 ) ) ;
#56436=EDGE_LOOP ( 'NONE', ( #39550, #100332, #65045, #74306 ) ) ;
#56439=CARTESIAN_POINT ( 'NONE',  ( -70.62287095715005592, -29.50247984919015209, -1.443849546365055359 ) ) ;
#56441=EDGE_LOOP ( 'NONE', ( #51294, #62100, #63834, #29730 ) ) ;
#56442=ORIENTED_EDGE ( 'NONE', *, *, #4776, .T. ) ;
#56444=CARTESIAN_POINT ( 'NONE',  ( -81.62287095715012697, -23.95044443724992789, 10.65354141964649592 ) ) ;
#56445=CARTESIAN_POINT ( 'NONE',  ( -55.58953762381671737, -24.99156044556120193, 7.747789690856344613 ) ) ;
#56446=CARTESIAN_POINT ( 'NONE',  ( -55.52287095715006870, -29.50250786944525672, 11.44777988621623876 ) ) ;
#56447=CARTESIAN_POINT ( 'NONE',  ( -19.59449498831206782, -6.737714454370689054, -1.500000000000002220 ) ) ;
#56448=ADVANCED_FACE ( 'NONE', ( #63395 ), #24798, .T. ) ;
#56449=CARTESIAN_POINT ( 'NONE',  ( 20.55956107658784404, -6.795330137259728787, 11.49999999999999645 ) ) ;
#56451=CARTESIAN_POINT ( 'NONE',  ( -110.6228709571500559, -25.00158670708909625, 2.256160236439165967 ) ) ;
#56452=LINE ( 'NONE', #78746, #7483 ) ;
#56453=CARTESIAN_POINT ( 'NONE',  ( 0.2029947971921062799, -22.41465419638480228, -1.500000000000002220 ) ) ;
#56454=VECTOR ( 'NONE', #14057, 1000.000000000000114 ) ;
#56455=CARTESIAN_POINT ( 'NONE',  ( -47.56853656710128320, -23.48786465467240347, 11.44779295918255002 ) ) ;
#56456=CARTESIAN_POINT ( 'NONE',  ( -102.5228709571501042, -24.35013146730204170, 9.818937971375097717 ) ) ;
#56458=CARTESIAN_POINT ( 'NONE',  ( -31.62287095715005947, -24.51387760970723662, 9.387446482453421837 ) ) ;
#56459=CARTESIAN_POINT ( 'NONE',  ( -35.64594292568924772, -24.40133493613049609, 9.663955038902800609 ) ) ;
#56460=ORIENTED_EDGE ( 'NONE', *, *, #29430, .T. ) ;
#56461=ORIENTED_EDGE ( 'NONE', *, *, #35399, .F. ) ;
#56462=CARTESIAN_POINT ( 'NONE',  ( -109.9228709571500531, -23.47596703998600631, 11.44779298504227860 ) ) ;
#56463=EDGE_CURVE ( 'NONE', #64065, #86743, #93307, .T. ) ;
#56465=FACE_OUTER_BOUND ( 'NONE', #75648, .T. ) ;
#56466=CARTESIAN_POINT ( 'NONE',  ( 17.81766572339076404, -11.58780717566545526, -1.500000000000002220 ) ) ;
#56467=EDGE_CURVE ( 'NONE', #35231, #83907, #55777, .T. ) ;
#56468=ORIENTED_EDGE ( 'NONE', *, *, #69398, .T. ) ;
#56470=CARTESIAN_POINT ( 'NONE',  ( 6.711561834375728175, -20.75310922853297058, 11.49999999999998934 ) ) ;
#56471=CARTESIAN_POINT ( 'NONE',  ( -103.5574460374484289, -23.73791477778911840, 11.05961554403170410 ) ) ;
#56474=CARTESIAN_POINT ( 'NONE',  ( -35.52287095715006870, -24.99156044556120193, 7.747789690856173195 ) ) ;
#56475=CARTESIAN_POINT ( 'NONE',  ( -18.33957545910867282, 11.93505917737106259, -1.500000000000002220 ) ) ;
#56476=CARTESIAN_POINT ( 'NONE',  ( -30.57287095715007297, -24.48748619694336881, 9.410756961485560623 ) ) ;
#56477=VERTEX_POINT ( 'NONE', #47658 ) ;
#56478=CARTESIAN_POINT ( 'NONE',  ( -69.62287095715004170, -23.96127896941632685, -0.6493128931037859264 ) ) ;
#56479=B_SPLINE_CURVE_WITH_KNOTS ( 'NONE', 3,
 ( #2110, #16810, #25427, #8709, #64528, #10207, #33544, #47775 ),
 .UNSPECIFIED., .F., .F.,
 ( 4, 2, 2, 4 ),
 ( 1.390486644391990834E-17, 0.0002557425425658982343, 0.0005114850851317825908, 0.001022970170263591419 ),
 .UNSPECIFIED. ) ;
#56480=CARTESIAN_POINT ( 'NONE',  ( -85.50609027866678957, -24.40133493613049964, 9.663955038902802386 ) ) ;
#56483=EDGE_CURVE ( 'NONE', #80790, #20207, #39810, .T. ) ;
#56486=VECTOR ( 'NONE', #8591, 1000.000000000000114 ) ;
#56487=ORIENTED_EDGE ( 'NONE', *, *, #52029, .T. ) ;
#56488=CARTESIAN_POINT ( 'NONE',  ( -83.52287095715007581, -23.48783264082477018, -1.443836473390090802 ) ) ;
#56489=CARTESIAN_POINT ( 'NONE',  ( -82.54713402157328517, -24.34968618360933945, 0.1864209137778926328 ) ) ;
#56490=CARTESIAN_POINT ( 'NONE',  ( 12.23393567461250697, 17.36540613969008007, 11.49999999999998934 ) ) ;
#56491=FACE_OUTER_BOUND ( 'NONE', #64236, .T. ) ;
#56492=CARTESIAN_POINT ( 'NONE',  ( -130.5728709571500588, -24.77158516743338623, 8.907023374642852431 ) ) ;
#56494=CARTESIAN_POINT ( 'NONE',  ( -99.52287095715010423, -23.94994826722565406, -0.6494450866342716955 ) ) ;
#56495=CARTESIAN_POINT ( 'NONE',  ( 19.38287969867323213, 0.6573286442255052986, 11.49999999999998934 ) ) ;
#56496=CARTESIAN_POINT ( 'NONE',  ( -45.47440205232901889, -24.92564183028978775, 1.928384488918256645 ) ) ;
#56498=CARTESIAN_POINT ( 'NONE',  ( 18.45204572605500104, 6.281640480902235701, 11.49999999999999645 ) ) ;
#56501=VERTEX_POINT ( 'NONE', #16187 ) ;
#56504=CARTESIAN_POINT ( 'NONE',  ( -90.52287095715006160, -24.15431212366388181, -0.2830839119429129913 ) ) ;
#56506=CARTESIAN_POINT ( 'NONE',  ( 19.58216393897113505, 1.562425146961006650, 11.49999999999998934 ) ) ;
#56508=DIRECTION ( 'NONE',  ( -1.000000000000000000, -3.773278334444167608E-23, -8.201307833595939069E-29 ) ) ;
#56509=CARTESIAN_POINT ( 'NONE',  ( 11.81885653190370888, -19.86314957129924608, -1.500000000000002220 ) ) ;
#56511=CARTESIAN_POINT ( 'NONE',  ( -106.5228709571500758, -24.64965694238408034, 8.947790433994192938 ) ) ;
#56513=CARTESIAN_POINT ( 'NONE',  ( -115.6228709571500417, -25.00182538069145721, 7.747789668545097541 ) ) ;
#56514=DIRECTION ( 'NONE',  ( -3.773278334453079618E-23, 0.9999999999976377785, 2.173523156925979975E-06 ) ) ;
#56515=CARTESIAN_POINT ( 'NONE',  ( -79.92244018840227682, -25.03722721891040948, 7.590183713343858329 ) ) ;
#56516=AXIS2_PLACEMENT_3D ( 'NONE', #30493, #46732, #77658 ) ;
#56517=CARTESIAN_POINT ( 'NONE',  ( -44.52287095715004028, -23.73907113216988307, -1.053371485793254347 ) ) ;
#56520=CARTESIAN_POINT ( 'NONE',  ( -16.62890364678930410, -10.96057169749504645, 11.49999999999998934 ) ) ;
#56521=CARTESIAN_POINT ( 'NONE',  ( -75.58919500596368835, -24.52399227489127043, 9.353111116836526406 ) ) ;
#56522=CARTESIAN_POINT ( 'NONE',  ( -10.02925392579303576, -17.20239368982820238, -1.500000000000002220 ) ) ;
#56525=CARTESIAN_POINT ( 'NONE',  ( -122.5228709571500616, -23.47596703998600631, 11.44779298504227860 ) ) ;
#56526=CARTESIAN_POINT ( 'NONE',  ( -101.6228709571500559, -24.64898659630368627, 1.056161002820829697 ) ) ;
#56527=CARTESIAN_POINT ( 'NONE',  ( -35.62287095715007013, -24.14406661707770496, 10.28769366152060982 ) ) ;
#56528=CARTESIAN_POINT ( 'NONE',  ( 18.03836333725549324, -10.36167025447706713, 11.49999999999999645 ) ) ;
#56531=CARTESIAN_POINT ( 'NONE',  ( -106.5562042904834072, -24.66019654487199730, 8.947790411086124607 ) ) ;
#56532=CARTESIAN_POINT ( 'NONE',  ( 17.57702471007113232, 14.52005670271990034, 11.49999999999999645 ) ) ;
#56533=ORIENTED_EDGE ( 'NONE', *, *, #73141, .F. ) ;
#56534=EDGE_CURVE ( 'NONE', #80860, #81148, #2268, .T. ) ;
#56536=CARTESIAN_POINT ( 'NONE',  ( -127.6248233915099917, -23.48783264082477018, -1.443836473390083919 ) ) ;
#56539=CARTESIAN_POINT ( 'NONE',  ( -19.33604739795523741, 5.927148246271303655, -1.500000000000002220 ) ) ;
#56544=CARTESIAN_POINT ( 'NONE',  ( -84.52287095715004739, -23.94994826722565406, -0.6494450866342729167 ) ) ;
#56545=EDGE_CURVE ( 'NONE', #57700, #11900, #89423, .T. ) ;
#56546=VERTEX_POINT ( 'NONE', #42552 ) ;
#56547=CARTESIAN_POINT ( 'NONE',  ( -0.1469190486835098564, -21.14801745985730719, -1.461890965025842704 ) ) ;
#56549=CARTESIAN_POINT ( 'NONE',  ( -7.473237707827510512, 18.53023608995856009, -1.500000000000002220 ) ) ;
#56551=CARTESIAN_POINT ( 'NONE',  ( 16.30764028314251846, 13.22082560946828522, 11.49999999999999645 ) ) ;
#56552=ADVANCED_FACE ( 'NONE', ( #11084 ), #57772, .F. ) ;
#56554=CARTESIAN_POINT ( 'NONE',  ( -70.53235729249159647, -25.00182538069146787, 7.747789668545044250 ) ) ;
#56555=CARTESIAN_POINT ( 'NONE',  ( -10.28628152547328511, -19.52461415289770130, 11.49999999999998934 ) ) ;
#56561=ORIENTED_EDGE ( 'NONE', *, *, #1862, .F. ) ;
#56562=DIRECTION ( 'NONE',  ( 0.000000000000000000, -0.9999999999976377785, -2.173523156925979128E-06 ) ) ;
#56563=ORIENTED_EDGE ( 'NONE', *, *, #1901, .T. ) ;
#56564=ORIENTED_EDGE ( 'NONE', *, *, #52896, .T. ) ;
#56565=CARTESIAN_POINT ( 'NONE',  ( -90.52287095715006160, -29.50250243563736774, 8.947779886222139822 ) ) ;
#56566=DIRECTION ( 'NONE',  ( -1.000000000000000000, -3.773278334444167608E-23, -8.201307833595939069E-29 ) ) ;
#56567=CARTESIAN_POINT ( 'NONE',  ( -94.62287095715011276, -23.95044443724992789, 10.65354141964649592 ) ) ;
#56568=CARTESIAN_POINT ( 'NONE',  ( 7.908618202329199320, -18.92053725880622039, -1.500000000000002220 ) ) ;
#56569=EDGE_CURVE ( 'NONE', #6577, #27644, #70003, .T. ) ;
#56570=ORIENTED_EDGE ( 'NONE', *, *, #25796, .T. ) ;
#56573=DIRECTION ( 'NONE',  ( -3.773278334453079618E-23, 0.9999999999976377785, 2.173523156925979975E-06 ) ) ;
#56574=CARTESIAN_POINT ( 'NONE',  ( -15.79502933763849271, 15.79022959414610661, -1.500000000000002220 ) ) ;
#56575=CARTESIAN_POINT ( 'NONE',  ( -0.02085506613324774119, -22.78001478014103398, 7.291654623549858272 ) ) ;
#56576=CARTESIAN_POINT ( 'NONE',  ( -90.58953762381671027, -24.99156044556120193, 7.747789690856343725 ) ) ;
#56579=CARTESIAN_POINT ( 'NONE',  ( -42.62287095715004881, -23.72747288104441665, -1.053458166803663110 ) ) ;
#56580=PLANE ( 'NONE',  #15107 ) ;
#56581=CARTESIAN_POINT ( 'NONE',  ( -0.6367455441941621830, -20.85161220577290919, -1.500000000000002220 ) ) ;
#56582=B_SPLINE_CURVE_WITH_KNOTS ( 'NONE', 3,
 ( #29034, #5205, #13801, #44776, #90441, #59010 ),
 .UNSPECIFIED., .F., .F.,
 ( 4, 2, 4 ),
 ( 1.570887131794333942E-05, 0.001396322306279759555, 0.002776935741241575838 ),
 .UNSPECIFIED. ) ;
#56583=ORIENTED_EDGE ( 'NONE', *, *, #38247, .F. ) ;
#56585=ADVANCED_FACE ( 'NONE', ( #50648 ), #73986, .T. ) ;
#56586=VERTEX_POINT ( 'NONE', #33926 ) ;
#56588=LINE ( 'NONE', #40838, #77826 ) ;
#56589=CARTESIAN_POINT ( 'NONE',  ( -20.60145385712877797, -4.430719527714695793, -1.500000000000002220 ) ) ;
#56590=ORIENTED_EDGE ( 'NONE', *, *, #39138, .F. ) ;
#56591=CARTESIAN_POINT ( 'NONE',  ( -93.62287095715014118, -24.35013146730204525, 9.818937971375106599 ) ) ;
#56593=CARTESIAN_POINT ( 'NONE',  ( -49.62788239718302918, -25.30563260921435997, 5.001563845361221894 ) ) ;
#56594=PLANE ( 'NONE',  #83747 ) ;
#56596=CARTESIAN_POINT ( 'NONE',  ( -86.52215071448813433, -23.48786465467241058, 11.44779295918254647 ) ) ;
#56598=CARTESIAN_POINT ( 'NONE',  ( 16.98214085172422827, 13.50221961261776293, -1.500000000000002220 ) ) ;
#56599=CARTESIAN_POINT ( 'NONE',  ( -64.52287095715009002, -23.72773821059535848, 11.05748984161097503 ) ) ;
#56600=CARTESIAN_POINT ( 'NONE',  ( 10.78255534502030777, 19.45608938089507234, 11.49999999999999645 ) ) ;
#56604=ORIENTED_EDGE ( 'NONE', *, *, #22669, .T. ) ;
#56605=AXIS2_PLACEMENT_3D ( 'NONE', #26851, #42092, #27353 ) ;
#56606=EDGE_CURVE ( 'NONE', #35091, #68548, #64906, .T. ) ;
#56610=VECTOR ( 'NONE', #44177, 1000.000000000000114 ) ;
#56613=CARTESIAN_POINT ( 'NONE',  ( -17.93149374516376682, -9.230432107326475233, 11.49999999999998934 ) ) ;
#56615=ORIENTED_EDGE ( 'NONE', *, *, #19463, .F. ) ;
#56616=VECTOR ( 'NONE', #54183, 1000.000000000000114 ) ;
#56617=CARTESIAN_POINT ( 'NONE',  ( -130.5728709571500588, -25.16880041465311990, 7.429836627804590421 ) ) ;
#56618=CARTESIAN_POINT ( 'NONE',  ( 15.34105849444754455, 16.31744944422920440, -1.500000000000002220 ) ) ;
#56619=ORIENTED_EDGE ( 'NONE', *, *, #26447, .T. ) ;
#56622=CARTESIAN_POINT ( 'NONE',  ( -101.5168322432302261, -23.96169478059713853, 10.65365249895717881 ) ) ;
#56623=CARTESIAN_POINT ( 'NONE',  ( -39.99371170946986354, -25.31560150972321921, 5.007528838953862582 ) ) ;
#56625=CARTESIAN_POINT ( 'NONE',  ( -63.90635932737072267, -25.30557784678704181, 3.856996771331004048 ) ) ;
#56626=CARTESIAN_POINT ( 'NONE',  ( -18.23851433863309879, 7.102826447048048664, -1.500000000000002220 ) ) ;
#56628=ORIENTED_EDGE ( 'NONE', *, *, #93777, .T. ) ;
#56629=CARTESIAN_POINT ( 'NONE',  ( -11.74548148041400708, 18.04809798412036059, -1.500000000000002220 ) ) ;
#56631=CARTESIAN_POINT ( 'NONE',  ( -71.23336565260535735, -25.25639482125388824, 6.552467071241729002 ) ) ;
#56632=DIRECTION ( 'NONE',  ( -3.773278334453079618E-23, 0.9999999999976377785, 2.173523156925979975E-06 ) ) ;
#56634=CARTESIAN_POINT ( 'NONE',  ( -10.62949710387652758, 20.32685691788189075, -1.500000000000002220 ) ) ;
#56636=CARTESIAN_POINT ( 'NONE',  ( -92.55620429048339304, -23.47593901973091235, -1.443836447539002865 ) ) ;
#56638=CARTESIAN_POINT ( 'NONE',  ( -20.09103079077430820, 1.113595961413322177, 11.49999999999999645 ) ) ;
#56639=CARTESIAN_POINT ( 'NONE',  ( -110.1676456071266870, -25.10927397016051543, 2.835829822663707755 ) ) ;
#56640=CARTESIAN_POINT ( 'NONE',  ( -31.52287095715006870, -24.34917612407033261, 0.1852690917477747279 ) ) ;
#56641=CARTESIAN_POINT ( 'NONE',  ( -121.6228709571499706, -24.33927499327854704, 9.819080762295808285 ) ) ;
#56642=CARTESIAN_POINT ( 'NONE',  ( -54.62287095715005592, -29.50250243563736774, 8.947779886222146928 ) ) ;
#56643=B_SPLINE_CURVE_WITH_KNOTS ( 'NONE', 3,
 ( #66029, #41168, #98424, #66529 ),
 .UNSPECIFIED., .F., .F.,
 ( 4, 4 ),
 ( 0.000000000000000000, 9.999999999998897304E-05 ),
 .UNSPECIFIED. ) ;
#56644=CARTESIAN_POINT ( 'NONE',  ( -126.5562042904833930, -24.64965694238575011, 8.947790433994191162 ) ) ;
#56645=CARTESIAN_POINT ( 'NONE',  ( 13.50462702941046977, 14.53317887778067252, 11.49999999999998934 ) ) ;
#56647=CARTESIAN_POINT ( 'NONE',  ( 16.91694316922610497, -9.995573847407506207, -1.500000000000002220 ) ) ;
#56651=CARTESIAN_POINT ( 'NONE',  ( -60.52287095715005449, -24.51254535375846189, 9.355368624242151654 ) ) ;
#56652=DIRECTION ( 'NONE',  ( -3.773278334453079030E-23, 0.9999999999976377785, 2.173523156925979128E-06 ) ) ;
#56653=CARTESIAN_POINT ( 'NONE',  ( 4.765357849511589805, 20.07956653139741121, 11.49999999999999645 ) ) ;
#56656=CARTESIAN_POINT ( 'NONE',  ( -2.075279548881721947, -22.52154899835045043, 11.49999999999999645 ) ) ;
#56657=ORIENTED_EDGE ( 'NONE', *, *, #91014, .F. ) ;
#56658=CARTESIAN_POINT ( 'NONE',  ( -69.34303308397305443, -25.25639407517101276, 6.209207384461285173 ) ) ;
#56660=EDGE_CURVE ( 'NONE', #64167, #100229, #79707, .T. ) ;
#56661=CARTESIAN_POINT ( 'NONE',  ( -100.6814946224345846, -25.31401921878175898, 5.197788989978544549 ) ) ;
#56665=EDGE_CURVE ( 'NONE', #65090, #61812, #84555, .T. ) ;
#56667=AXIS2_PLACEMENT_3D ( 'NONE', #60453, #27988, #91373 ) ;
#56668=EDGE_CURVE ( 'NONE', #48696, #39695, #36232, .T. ) ;
#56669=VERTEX_POINT ( 'NONE', #27308 ) ;
#56670=CARTESIAN_POINT ( 'NONE',  ( -80.43221577628075636, -25.31596222142643171, 4.967019754985606106 ) ) ;
#56671=CARTESIAN_POINT ( 'NONE',  ( -0.7673284989158746239, 22.82873350090251918, 11.49999999999998934 ) ) ;
#56672=CARTESIAN_POINT ( 'NONE',  ( -91.62287095715004170, -29.50247984919015209, -1.443849546365051806 ) ) ;
#56674=LINE ( 'NONE', #18091, #31751 ) ;
#56676=CARTESIAN_POINT ( 'NONE',  ( -6.716530693746936898, -21.44081863256500142, 11.49999999999999645 ) ) ;
#56680=B_SPLINE_CURVE_WITH_KNOTS ( 'NONE', 3,
 ( #37552, #99437, #12204, #84213, #81340, #23818 ),
 .UNSPECIFIED., .F., .F.,
 ( 4, 2, 4 ),
 ( 0.000000000000000000, 0.001380764517853246432, 0.002761529035706492864 ),
 .UNSPECIFIED. ) ;
#56681=CARTESIAN_POINT ( 'NONE',  ( 1.410849576418898632, -21.91845101833037290, -1.500000000000002220 ) ) ;
#56682=LINE ( 'NONE', #94716, #93239 ) ;
#56683=VECTOR ( 'NONE', #49874, 1000.000000000000114 ) ;
#56684=CARTESIAN_POINT ( 'NONE',  ( -34.65814782573328046, -23.73791477778911485, 11.05961554403171299 ) ) ;
#56685=CARTESIAN_POINT ( 'NONE',  ( -112.5228709571500616, -24.64965694238408034, 8.947790433994192938 ) ) ;
#56688=CARTESIAN_POINT ( 'NONE',  ( -112.5562042904834072, -23.48786465467241769, 11.44779295918253581 ) ) ;
#56689=DIRECTION ( 'NONE',  ( -3.773278334453079030E-23, 0.9999999999976377785, 2.173523156925979128E-06 ) ) ;
#56690=ORIENTED_EDGE ( 'NONE', *, *, #97429, .T. ) ;
#56691=CARTESIAN_POINT ( 'NONE',  ( -105.6228709571500559, -23.48783264082479150, -1.443836473390060160 ) ) ;
#56692=CARTESIAN_POINT ( 'NONE',  ( 19.83930831332124001, -5.160774681608516268, -1.500000000000002220 ) ) ;
#56693=ORIENTED_EDGE ( 'NONE', *, *, #70392, .T. ) ;
#56696=ORIENTED_EDGE ( 'NONE', *, *, #18083, .F. ) ;
#56698=CARTESIAN_POINT ( 'NONE',  ( 21.06059016766346659, 9.494407541345388779, 11.49999999999998934 ) ) ;
#56699=CARTESIAN_POINT ( 'NONE',  ( -104.5858001345268349, -24.66019654487200441, 8.947790411086108620 ) ) ;
#56700=CARTESIAN_POINT ( 'NONE',  ( 8.409737122318338365, 18.51778827956368190, -1.500000000000002220 ) ) ;
#56701=ORIENTED_EDGE ( 'NONE', *, *, #38202, .T. ) ;
#56703=CARTESIAN_POINT ( 'NONE',  ( -50.54485904939332386, -25.12158324412746424, 2.838362104969525124 ) ) ;
#56704=CARTESIAN_POINT ( 'NONE',  ( -101.5468792378191836, -25.25287247409163527, 6.236250661346386615 ) ) ;
#56706=ORIENTED_EDGE ( 'NONE', *, *, #40806, .T. ) ;
#56707=CARTESIAN_POINT ( 'NONE',  ( -29.24636659181000198, -25.21532237603348037, 4.940287017762114985 ) ) ;
#56708=CARTESIAN_POINT ( 'NONE',  ( -49.14050969713319716, -25.31573689518325310, 4.284284265464324726 ) ) ;
#56709=ORIENTED_EDGE ( 'NONE', *, *, #98216, .T. ) ;
#56710=CARTESIAN_POINT ( 'NONE',  ( -18.78340662496949776, 8.880393494302802893, 11.49999999999998934 ) ) ;
#56711=VERTEX_POINT ( 'NONE', #14062 ) ;
#56712=CARTESIAN_POINT ( 'NONE',  ( -125.5194286696376338, -24.92564183028979485, 1.928384488918254425 ) ) ;
#56716=ORIENTED_EDGE ( 'NONE', *, *, #2074, .F. ) ;
#56717=ORIENTED_EDGE ( 'NONE', *, *, #66528, .T. ) ;
#56719=CARTESIAN_POINT ( 'NONE',  ( -98.55620429048339304, -23.48786465467241769, 11.44779295918253759 ) ) ;
#56720=CARTESIAN_POINT ( 'NONE',  ( -78.52287095715006160, -23.72747288104470087, -1.053458166803226126 ) ) ;
#56721=CARTESIAN_POINT ( 'NONE',  ( -0.5447568859041533873, -22.05808898580190558, 11.49999999999999645 ) ) ;
#56722=ORIENTED_EDGE ( 'NONE', *, *, #96979, .T. ) ;
#56723=CARTESIAN_POINT ( 'NONE',  ( -108.6335339856925799, -23.48783264082478794, -1.443836473390062825 ) ) ;
#56724=CARTESIAN_POINT ( 'NONE',  ( 15.88279217892459094, 16.07415641707351384, 11.49999999999998934 ) ) ;
#56725=B_SPLINE_CURVE_WITH_KNOTS ( 'NONE', 3,
 ( #12307, #96555, #10828, #88956, #95562, #49407 ),
 .UNSPECIFIED., .F., .F.,
 ( 4, 2, 4 ),
 ( 0.000000000000000000, 0.001380764517854764749, 0.002761529035709529498 ),
 .UNSPECIFIED. ) ;
#56726=ADVANCED_FACE ( 'NONE', ( #76457 ), #45536, .F. ) ;
#56730=DIRECTION ( 'NONE',  ( 1.000000000000000000, 3.773278334444167608E-23, 8.201307833595939069E-29 ) ) ;
#56732=EDGE_CURVE ( 'NONE', #61820, #37466, #8364, .T. ) ;
#56733=CARTESIAN_POINT ( 'NONE',  ( -94.62287095715005592, -24.64898659630528854, 1.056161002820827921 ) ) ;
#56734=VERTEX_POINT ( 'NONE', #67875 ) ;
#56735=CARTESIAN_POINT ( 'NONE',  ( -4.955175619359221351, 20.59750927568439138, -1.500000000000002220 ) ) ;
#56736=CARTESIAN_POINT ( 'NONE',  ( -66.62287095715005592, -23.72773821059535493, 11.05748984161097681 ) ) ;
#56737=DIRECTION ( 'NONE',  ( 0.000000000000000000, 0.000000000000000000, 1.000000000000000000 ) ) ;
#56740=CARTESIAN_POINT ( 'NONE',  ( -41.73352883455704898, -25.30440811136059764, 4.814461953015128692 ) ) ;
#56741=CARTESIAN_POINT ( 'NONE',  ( -7.359855604737914447, 20.98419016808480109, -1.500000000000002220 ) ) ;
#56742=B_SPLINE_CURVE_WITH_KNOTS ( 'NONE', 3,
 ( #59831, #21241, #91261, #91752 ),
 .UNSPECIFIED., .F., .F.,
 ( 4, 4 ),
 ( 0.000000000000000000, 9.999999999998897304E-05 ),
 .UNSPECIFIED. ) ;
#56743=CARTESIAN_POINT ( 'NONE',  ( -114.5511112493029344, -24.65952944569305316, 1.056160979905706121 ) ) ;
#56744=ORIENTED_EDGE ( 'NONE', *, *, #38707, .F. ) ;
#56745=DIRECTION ( 'NONE',  ( -3.773278334453079030E-23, 0.9999999999976377785, 2.173523156925978705E-06 ) ) ;
#56747=CARTESIAN_POINT ( 'NONE',  ( -7.246369895950522277, -17.95243785538732340, 11.49999999999999645 ) ) ;
#56749=CARTESIAN_POINT ( 'NONE',  ( -71.55620429048339304, -23.48783264082478084, -1.443836473390067265 ) ) ;
#56750=CARTESIAN_POINT ( 'NONE',  ( -116.6228709571500559, -24.64898659630368627, 1.056161002820833028 ) ) ;
#56752=CARTESIAN_POINT ( 'NONE',  ( 19.40022266231057202, 1.907866353064612053, -1.500000000000002220 ) ) ;
#56753=VECTOR ( 'NONE', #82359, 1000.000000000000114 ) ;
#56754=CARTESIAN_POINT ( 'NONE',  ( 1.185105815240312888, -21.37944065014308848, -1.500000000000002220 ) ) ;
#56755=CARTESIAN_POINT ( 'NONE',  ( -32.52287095715006160, -24.64965694238575011, 8.947790433994207149 ) ) ;
#56756=CARTESIAN_POINT ( 'NONE',  ( -60.51213338828525679, -23.85049219812968957, 10.88485053497088728 ) ) ;
#56757=CARTESIAN_POINT ( 'NONE',  ( -51.49552821830581451, -24.34968618360933590, 0.1864209137778788938 ) ) ;
#56758=CARTESIAN_POINT ( 'NONE',  ( -120.6228709571500417, -24.99156045073393528, 7.747789690856161648 ) ) ;
#56759=CARTESIAN_POINT ( 'NONE',  ( 7.533951754900199305, 21.46025436219600024, -1.500000000000002220 ) ) ;
#56761=CARTESIAN_POINT ( 'NONE',  ( -98.54623345124143441, -24.65952944569305316, 1.056160979905702124 ) ) ;
#56762=CARTESIAN_POINT ( 'NONE',  ( -80.52287095715003318, -23.84047902841601996, -0.8780736468305722076 ) ) ;
#56763=CARTESIAN_POINT ( 'NONE',  ( 11.60740158406642664, -16.16820694497113564, 11.49999999999999645 ) ) ;
#56764=DIRECTION ( 'NONE',  ( 0.000000000000000000, 0.9999999999976377785, 2.173523156925979128E-06 ) ) ;
#56765=B_SPLINE_CURVE_WITH_KNOTS ( 'NONE', 3,
 ( #32822, #9480, #92211, #366, #85100, #8484 ),
 .UNSPECIFIED., .F., .F.,
 ( 4, 2, 4 ),
 ( 0.000000000000000000, 0.001380901958385381606, 0.002761803916770763211 ),
 .UNSPECIFIED. ) ;
#56766=CARTESIAN_POINT ( 'NONE',  ( -39.52823043622210974, -24.66019654487198665, 8.947790411086131712 ) ) ;
#56767=CARTESIAN_POINT ( 'NONE',  ( -112.5228709571500616, -29.50247984919015209, -1.443849546365048253 ) ) ;
#56769=CARTESIAN_POINT ( 'NONE',  ( -93.62287095715005592, -29.50247984919015209, -1.443849546365051806 ) ) ;
#56771=CARTESIAN_POINT ( 'NONE',  ( -12.04083774165243881, -18.01462592983040523, -1.500000000000002220 ) ) ;
#56772=FACE_OUTER_BOUND ( 'NONE', #67340, .T. ) ;
#56773=CARTESIAN_POINT ( 'NONE',  ( 8.422564666779264186, -17.53554878399664574, -1.500000000000002220 ) ) ;
#56774=CARTESIAN_POINT ( 'NONE',  ( -93.52287095715011844, -23.96127896941631974, -0.6493128931038023577 ) ) ;
#56775=ORIENTED_EDGE ( 'NONE', *, *, #12075, .T. ) ;
#56777=CARTESIAN_POINT ( 'NONE',  ( -20.32544160278596834, -1.370942541838689799, 11.49999999999999645 ) ) ;
#56779=B_SPLINE_CURVE_WITH_KNOTS ( 'NONE', 3,
 ( #57598, #96633, #49989, #26130, #4299, #11901 ),
 .UNSPECIFIED., .F., .F.,
 ( 4, 2, 4 ),
 ( 1.570887131794333942E-05, 0.001396322306279758037, 0.002776935741241572803 ),
 .UNSPECIFIED. ) ;
#56780=CARTESIAN_POINT ( 'NONE',  ( -86.55620429048339304, -24.64965694238575011, 8.947790433994194714 ) ) ;
#56782=CARTESIAN_POINT ( 'NONE',  ( -72.52287095715010423, -23.48783264082476308, -1.443836473390092578 ) ) ;
#56783=PLANE ( 'NONE',  #29867 ) ;
#56784=CARTESIAN_POINT ( 'NONE',  ( -39.04303308397306438, -25.31628448545684407, 4.215216869667997024 ) ) ;
#56785=EDGE_CURVE ( 'NONE', #82541, #59433, #31370, .T. ) ;
#56786=CARTESIAN_POINT ( 'NONE',  ( -49.45828852499023753, -25.25138767200333589, 5.632645021930186680 ) ) ;
#56787=CARTESIAN_POINT ( 'NONE',  ( -129.5228709571499905, -23.48783264082477729, -1.443836473390079700 ) ) ;
#56788=CARTESIAN_POINT ( 'NONE',  ( -109.5167418412546709, -24.15543982623907482, -0.2315651400026587370 ) ) ;
#56791=CARTESIAN_POINT ( 'NONE',  ( -66.64101351466018741, -23.96169478059713143, 10.65365249895718058 ) ) ;
#56792=EDGE_CURVE ( 'NONE', #50913, #70837, #47006, .T. ) ;
#56793=CARTESIAN_POINT ( 'NONE',  ( 22.85142058292489153, -2.183311388647848350, 11.49999999999999645 ) ) ;
#56794=CARTESIAN_POINT ( 'NONE',  ( 22.69831151501224298, -1.600861625767590724, -1.500000000000002220 ) ) ;
#56796=EDGE_CURVE ( 'NONE', #26222, #46090, #60764, .T. ) ;
#56798=CARTESIAN_POINT ( 'NONE',  ( -90.58310404013386119, -24.92564183028979130, 1.928384488918253536 ) ) ;
#56800=CARTESIAN_POINT ( 'NONE',  ( -69.37501441204418029, -25.22917552048557965, 6.451241004143004609 ) ) ;
#56801=AXIS2_PLACEMENT_3D ( 'NONE', #71277, #32704, #94605 ) ;
#56802=CARTESIAN_POINT ( 'NONE',  ( -1.606994170628035068, 21.82944698466814870, -1.500000000000002220 ) ) ;
#56804=CARTESIAN_POINT ( 'NONE',  ( -26.76057841451696362, -24.78115552336511129, 2.652511023330785367 ) ) ;
#56806=CARTESIAN_POINT ( 'NONE',  ( -58.55359724368977936, -23.96119346886881019, -0.6495511937832116889 ) ) ;
#56807=ORIENTED_EDGE ( 'NONE', *, *, #43975, .F. ) ;
#56808=CARTESIAN_POINT ( 'NONE',  ( -14.48729221511043441, 14.40292172154154926, 11.49999999999998934 ) ) ;
#56811=EDGE_CURVE ( 'NONE', #63805, #20892, #4967, .T. ) ;
#56812=CARTESIAN_POINT ( 'NONE',  ( 3.792298468851710069, -22.70151372599487871, 11.49999999999998934 ) ) ;
#56813=CARTESIAN_POINT ( 'NONE',  ( -30.64427850938831099, -23.56000036390796382, 11.50200000000000067 ) ) ;
#56815=CARTESIAN_POINT ( 'NONE',  ( -108.5593205469241553, -23.48786465467241413, 11.44779295918253759 ) ) ;
#56816=DIRECTION ( 'NONE',  ( -3.773278334444167608E-23, 1.000000000000000000, 0.000000000000000000 ) ) ;
#56818=CARTESIAN_POINT ( 'NONE',  ( -62.52287095715006160, -29.50247984919015209, -1.443849546365056913 ) ) ;
#56819=CARTESIAN_POINT ( 'NONE',  ( -118.8950128664978507, -25.24724904090927424, 6.200150947452693018 ) ) ;
#56820=CARTESIAN_POINT ( 'NONE',  ( -21.27170209485220198, -2.091907790468015005, 11.49999999999999645 ) ) ;
#56821=ORIENTED_EDGE ( 'NONE', *, *, #64512, .T. ) ;
#56823=ORIENTED_EDGE ( 'NONE', *, *, #8646, .F. ) ;
#56824=CARTESIAN_POINT ( 'NONE',  ( -7.359855604737914447, 20.98419016808480109, -1.500000000000002220 ) ) ;
#56825=CARTESIAN_POINT ( 'NONE',  ( 3.345817365282868217, 20.41450801592841557, -1.500000000000002220 ) ) ;
#56826=AXIS2_PLACEMENT_3D ( 'NONE', #46744, #52357, #46236 ) ;
#56827=EDGE_LOOP ( 'NONE', ( #958, #42752, #39466, #20346 ) ) ;
#56831=DIRECTION ( 'NONE',  ( -9.524068072025174096E-40, -2.173523156925980399E-06, 0.9999999999976378895 ) ) ;
#56832=ORIENTED_EDGE ( 'NONE', *, *, #27260, .T. ) ;
#56834=CARTESIAN_POINT ( 'NONE',  ( -71.17423078786923440, -25.19025574039271831, 6.676846143341355067 ) ) ;
#56835=CARTESIAN_POINT ( 'NONE',  ( -11.21968731015968856, -17.59241007644406096, -1.500000000000002220 ) ) ;
#56836=CARTESIAN_POINT ( 'NONE',  ( 21.45948982579844255, -4.128456637845983934, 11.49999999999999645 ) ) ;
#56837=EDGE_CURVE ( 'NONE', #35259, #55090, #92992, .T. ) ;
#56839=CARTESIAN_POINT ( 'NONE',  ( -37.62287095715007013, -24.51283580621364777, 0.6167428607019709297 ) ) ;
#56840=CARTESIAN_POINT ( 'NONE',  ( 0.003324065884441271702, 22.49086686382009503, -1.500000000000002220 ) ) ;
#56841=CARTESIAN_POINT ( 'NONE',  ( -8.531171415479239073, -19.09552649099111221, 11.49999999999998934 ) ) ;
#56842=CARTESIAN_POINT ( 'NONE',  ( -26.15327376889522526, -24.88148900154536491, 5.797586012370106623 ) ) ;
#56848=EDGE_LOOP ( 'NONE', ( #81861, #59417, #83124, #61664 ) ) ;
#56851=CARTESIAN_POINT ( 'NONE',  ( -17.32345979880200204, -12.59856583755568415, -1.500000000000002220 ) ) ;
#56852=CARTESIAN_POINT ( 'NONE',  ( -15.72835732567950195, 15.92727474065614501, 11.49999999999999645 ) ) ;
#56853=EDGE_CURVE ( 'NONE', #55337, #21700, #10707, .T. ) ;
#56855=CARTESIAN_POINT ( 'NONE',  ( -26.12985137885329223, -24.94751919380807692, 5.610999066408565383 ) ) ;
#56856=CARTESIAN_POINT ( 'NONE',  ( -4.359323203648655998, -20.60729432550360585, -1.500000000000002220 ) ) ;
#56857=CARTESIAN_POINT ( 'NONE',  ( -30.47189344453343551, -23.47433389951690330, 11.44779287168131710 ) ) ;
#56858=CARTESIAN_POINT ( 'NONE',  ( 19.82558669001425500, -2.195561414069463702, -1.500000000000002220 ) ) ;
#56859=CARTESIAN_POINT ( 'NONE',  ( -50.58895421723637043, -24.52399227489127043, 9.353111116836521077 ) ) ;
#56860=CARTESIAN_POINT ( 'NONE',  ( -88.62287095715004170, -29.50250243563736774, 8.947779886222139822 ) ) ;
#56861=CARTESIAN_POINT ( 'NONE',  ( -21.70078857174656761, -3.768841730229552045, -1.500000000000002220 ) ) ;
#56862=VERTEX_POINT ( 'NONE', #83578 ) ;
#56863=CARTESIAN_POINT ( 'NONE',  ( -65.63574626809028700, -24.52399227489126687, 9.353111116836526406 ) ) ;
#56865=CARTESIAN_POINT ( 'NONE',  ( -93.62287095715005592, -29.50248528299804818, 1.056150453629040253 ) ) ;
#56866=CARTESIAN_POINT ( 'NONE',  ( -41.25901049487872996, -25.27956024727518525, 5.328837458236013624 ) ) ;
#56867=CARTESIAN_POINT ( 'NONE',  ( -29.83719645772528750, -25.26444761590789767, 6.075536601959948158 ) ) ;
#56868=CARTESIAN_POINT ( 'NONE',  ( -25.55992647825761566, -24.89300974704809022, 4.202247098034709971 ) ) ;
#56870=CARTESIAN_POINT ( 'NONE',  ( -6.620899627221215944, -20.26055204357936290, -1.500000000000002220 ) ) ;
#56871=CARTESIAN_POINT ( 'NONE',  ( -104.5228709571501327, -24.51387760970725438, 9.387446482453409402 ) ) ;
#56873=B_SPLINE_CURVE_WITH_KNOTS ( 'NONE', 3,
 ( #54900, #92439, #16323, #92938 ),
 .UNSPECIFIED., .F., .F.,
 ( 4, 4 ),
 ( 0.000000000000000000, 0.0004038461538461574074 ),
 .UNSPECIFIED. ) ;
#56876=DIRECTION ( 'NONE',  ( 3.773278334444167608E-23, -1.000000000000000000, 0.000000000000000000 ) ) ;
#56878=CARTESIAN_POINT ( 'NONE',  ( 20.74359285767136640, 8.971229656761206428, -1.500000000000002220 ) ) ;
#56879=CARTESIAN_POINT ( 'NONE',  ( -123.6228709571500559, -24.64898659630368627, 1.056161002820833028 ) ) ;
#56882=CARTESIAN_POINT ( 'NONE',  ( -122.6228709571500417, -24.33832256526969218, 0.1851278514119942820 ) ) ;
#56883=CARTESIAN_POINT ( 'NONE',  ( 3.553741186906278493, -19.43417129498564577, 11.49999999999999645 ) ) ;
#56885=CARTESIAN_POINT ( 'NONE',  ( -73.52287095715013265, -24.33927499327855770, 9.819080762295815390 ) ) ;
#56888=CARTESIAN_POINT ( 'NONE',  ( -124.4728709594060376, -25.21147767388034566, 8.000950762517446080 ) ) ;
#56889=CARTESIAN_POINT ( 'NONE',  ( -105.5228709571500758, -24.52323809116984421, 9.355190652339418378 ) ) ;
#56891=CARTESIAN_POINT ( 'NONE',  ( -95.52287095715003318, -23.85229601348997264, 10.88205029486208630 ) ) ;
#56892=CARTESIAN_POINT ( 'NONE',  ( -113.5228709571500616, -24.65952944569304961, 1.056160979905704123 ) ) ;
#56893=CARTESIAN_POINT ( 'NONE',  ( -18.42202159362721048, -7.168033771007030097, 11.49999999999998934 ) ) ;
#56894=B_SPLINE_CURVE_WITH_KNOTS ( 'NONE', 3,
 ( #63239, #85050, #31266, #46500 ),
 .UNSPECIFIED., .F., .F.,
 ( 4, 4 ),
 ( 0.000000000000000000, 9.999999999998897304E-05 ),
 .UNSPECIFIED. ) ;
#56895=VECTOR ( 'NONE', #69198, 1000.000000000000114 ) ;
#56896=EDGE_LOOP ( 'NONE', ( #53097, #8514, #55097, #20963 ) ) ;
#56898=CARTESIAN_POINT ( 'NONE',  ( 8.473373031455752269, -18.34320851062214430, 11.49999999999999645 ) ) ;
#56900=ORIENTED_EDGE ( 'NONE', *, *, #11170, .T. ) ;
#56902=CARTESIAN_POINT ( 'NONE',  ( -118.6228709571500559, -24.64898659630368627, 1.056161002820833028 ) ) ;
#56904=CARTESIAN_POINT ( 'NONE',  ( -97.62287095715005592, -29.50247984919015209, -1.443849546365050029 ) ) ;
#56905=CARTESIAN_POINT ( 'NONE',  ( -128.6228709571500417, -23.47593901973091235, -1.443836447538995760 ) ) ;
#56906=CARTESIAN_POINT ( 'NONE',  ( -96.52287095715001897, -24.34917612406836795, 0.1852690917426570161 ) ) ;
#56907=CARTESIAN_POINT ( 'NONE',  ( 12.85705330080557829, 15.37097598829428513, -1.500000000000002220 ) ) ;
#56909=CARTESIAN_POINT ( 'NONE',  ( -39.62287095715005592, -23.47596703998600276, 11.44779298504227505 ) ) ;
#56910=ORIENTED_EDGE ( 'NONE', *, *, #46466, .T. ) ;
#56912=EDGE_CURVE ( 'NONE', #77838, #7215, #84578, .T. ) ;
#56913=CARTESIAN_POINT ( 'NONE',  ( -35.51858042511292979, -25.00158670708910336, 2.256160236439224143 ) ) ;
#56914=CARTESIAN_POINT ( 'NONE',  ( -92.62287095715009855, -23.95044443724992789, 10.65354141964649948 ) ) ;
#56916=CARTESIAN_POINT ( 'NONE',  ( -113.5228709571500616, -23.47593901973090524, -1.443836447538996204 ) ) ;
#56917=CARTESIAN_POINT ( 'NONE',  ( -73.54184938391159676, -24.51314013834315375, 0.6176544820404108460 ) ) ;
#56918=CARTESIAN_POINT ( 'NONE',  ( -89.40841769935767047, -25.22391154813773895, 6.409327647370974823 ) ) ;
#56919=CARTESIAN_POINT ( 'NONE',  ( -49.56706780694642589, -25.23900318944143706, 3.731069057777267162 ) ) ;
#56920=ORIENTED_EDGE ( 'NONE', *, *, #65023, .T. ) ;
#56921=CARTESIAN_POINT ( 'NONE',  ( -20.26613141553852060, -1.498020344548873561, 11.49999999999998934 ) ) ;
#56923=B_SPLINE_CURVE_WITH_KNOTS ( 'NONE', 3,
 ( #39087, #62951, #55837, #47719 ),
 .UNSPECIFIED., .F., .F.,
 ( 4, 4 ),
 ( 0.000000000000000000, 9.999999999998897304E-05 ),
 .UNSPECIFIED. ) ;
#56925=CARTESIAN_POINT ( 'NONE',  ( -32.52200313167130474, -23.48783264082477729, -1.443836473390076147 ) ) ;
#56926=CARTESIAN_POINT ( 'NONE',  ( -127.6248241772779437, -23.48786465467242124, 11.44779295918253403 ) ) ;
#56928=FACE_OUTER_BOUND ( 'NONE', #6875, .T. ) ;
#56929=CARTESIAN_POINT ( 'NONE',  ( -49.31927893949910668, -25.26264030274095163, 6.419594040249337219 ) ) ;
#56930=CARTESIAN_POINT ( 'NONE',  ( -65.62287095715008434, -24.82576562982392687, 8.398263435472971494 ) ) ;
#56931=CARTESIAN_POINT ( 'NONE',  ( 10.59196434753715010, 18.29633683537252509, 11.49999999999999645 ) ) ;
#56932=CARTESIAN_POINT ( 'NONE',  ( 22.09269804725545683, -1.632937629565654580, 11.49999999999998934 ) ) ;
#56934=CARTESIAN_POINT ( 'NONE',  ( -20.17529555308526668, -4.016306826964139098, 11.49999999999998934 ) ) ;
#56935=ORIENTED_EDGE ( 'NONE', *, *, #24395, .F. ) ;
#56936=CARTESIAN_POINT ( 'NONE',  ( -41.49214519350802988, -24.34968618360933590, 0.1864209137778857495 ) ) ;
#56938=DIRECTION ( 'NONE',  ( 0.000000000000000000, 0.9999999999976377785, 2.173523156925979975E-06 ) ) ;
#56939=CARTESIAN_POINT ( 'NONE',  ( -61.62287095715007013, -24.35013146730203104, 9.818937971375115481 ) ) ;
#56941=ORIENTED_EDGE ( 'NONE', *, *, #89217, .F. ) ;
#56942=B_SPLINE_CURVE_WITH_KNOTS ( 'NONE', 3,
 ( #29514, #93410, #69594, #75682 ),
 .UNSPECIFIED., .F., .F.,
 ( 4, 4 ),
 ( 2.775557561562891043E-17, 9.999999999996124456E-05 ),
 .UNSPECIFIED. ) ;
#56947=CARTESIAN_POINT ( 'NONE',  ( -6.067718162532647064, 19.77315050736717694, -1.500000000000002220 ) ) ;
#56948=CARTESIAN_POINT ( 'NONE',  ( -0.4625342273119020797, 21.68341340789531912, 11.49999999999999645 ) ) ;
#56951=CARTESIAN_POINT ( 'NONE',  ( -111.4927656110371714, -25.20245619288051131, 3.420186212457718256 ) ) ;
#56952=CARTESIAN_POINT ( 'NONE',  ( -3.217810451210200817, -22.18463865543611391, -1.500000000000002220 ) ) ;
#56953=CARTESIAN_POINT ( 'NONE',  ( -124.6228709571500559, -23.48783264082479505, -1.443836473390058828 ) ) ;
#56954=CARTESIAN_POINT ( 'NONE',  ( -71.62287095715004170, -23.96127896941632685, -0.6493128931037889240 ) ) ;
#56955=EDGE_CURVE ( 'NONE', #27253, #35212, #39412, .T. ) ;
#56956=ORIENTED_EDGE ( 'NONE', *, *, #29886, .T. ) ;
#56959=CARTESIAN_POINT ( 'NONE',  ( -35.59333913237350089, -24.40133493613049609, 9.663955038902800609 ) ) ;
#56961=VERTEX_POINT ( 'NONE', #69362 ) ;
#56963=ORIENTED_EDGE ( 'NONE', *, *, #1952, .T. ) ;
#56966=CARTESIAN_POINT ( 'NONE',  ( -20.47598858559898716, 5.595549388561865456, -1.500000000000002220 ) ) ;
#56967=ORIENTED_EDGE ( 'NONE', *, *, #996, .F. ) ;
#56969=CARTESIAN_POINT ( 'NONE',  ( -12.45635911906152771, -17.91357634596933934, 11.49999999999998934 ) ) ;
#56970=CARTESIAN_POINT ( 'NONE',  ( -52.57794027106912438, -24.66019654487198665, 8.947790411086131712 ) ) ;
#56972=PLANE ( 'NONE',  #41726 ) ;
#56973=CARTESIAN_POINT ( 'NONE',  ( 21.45948982579844255, -4.128456637845983934, -1.500000000000002220 ) ) ;
#56974=CARTESIAN_POINT ( 'NONE',  ( -109.5228709571500758, -23.96177878511309345, 10.65340807706329329 ) ) ;
#56975=ORIENTED_EDGE ( 'NONE', *, *, #42811, .F. ) ;
#56977=CARTESIAN_POINT ( 'NONE',  ( -85.63196641622515415, -24.52399227489127043, 9.353111116836526406 ) ) ;
#56979=CARTESIAN_POINT ( 'NONE',  ( -30.60157315003009515, -24.66735617610590126, 1.103427580892887283 ) ) ;
#56982=CARTESIAN_POINT ( 'NONE',  ( -82.59550824821182857, -23.96119346886881019, -0.6495511937831922600 ) ) ;
#56983=CARTESIAN_POINT ( 'NONE',  ( 20.85495618715548716, -4.085033163991189653, -1.500000000000002220 ) ) ;
#56985=CARTESIAN_POINT ( 'NONE',  ( -130.5728709571500588, -24.87212640336025871, 1.420893871182737023 ) ) ;
#56986=EDGE_CURVE ( 'NONE', #86130, #35546, #3531, .T. ) ;
#56988=DIRECTION ( 'NONE',  ( 1.000000000000000000, 3.773278334444166432E-23, 8.201307841325785021E-29 ) ) ;
#56989=CARTESIAN_POINT ( 'NONE',  ( -1.307668758097810358, 19.38731951181482671, -1.500000000000002220 ) ) ;
#56992=VERTEX_POINT ( 'NONE', #23673 ) ;
#56993=CARTESIAN_POINT ( 'NONE',  ( -19.08498223313328168, 4.104482590468319536, 11.49999999999999645 ) ) ;
#56995=CARTESIAN_POINT ( 'NONE',  ( -29.52074223362913585, -25.06969336238594792, 6.937538283832196839 ) ) ;
#56996=B_SPLINE_CURVE_WITH_KNOTS ( 'NONE', 3,
 ( #46868, #33137, #685, #32132 ),
 .UNSPECIFIED., .F., .F.,
 ( 4, 4 ),
 ( 0.000000000000000000, 9.999999999998897304E-05 ),
 .UNSPECIFIED. ) ;
#56998=CARTESIAN_POINT ( 'NONE',  ( -58.62287095715006302, -23.95044443724992078, 10.65354141964650125 ) ) ;
#57000=CARTESIAN_POINT ( 'NONE',  ( -89.62850960197191341, -24.34968618360933945, 0.1864209137778942982 ) ) ;
#57001=ADVANCED_FACE ( 'NONE', ( #23164 ), #34439, .T. ) ;
#57003=CARTESIAN_POINT ( 'NONE',  ( -80.64549629918748508, -25.24813990744215886, 7.560538059850569148 ) ) ;
#57004=CARTESIAN_POINT ( 'NONE',  ( -0.7274468246531539117, 19.66889477801398911, -1.500000000000002220 ) ) ;
#57006=EDGE_LOOP ( 'NONE', ( #18492, #26506, #2688, #39310 ) ) ;
#57009=CARTESIAN_POINT ( 'NONE',  ( -114.5895376238167387, -23.47596703998600631, 11.44779298504227683 ) ) ;
#57012=CARTESIAN_POINT ( 'NONE',  ( -125.5228709571500616, -23.48786465467241769, 11.44779295918253581 ) ) ;
#57014=CARTESIAN_POINT ( 'NONE',  ( -115.6228709571500133, -24.63345952396256422, 9.038047939301501188 ) ) ;
#57015=CARTESIAN_POINT ( 'NONE',  ( -97.51107724223938078, -24.35071581493543746, 9.817618358456025263 ) ) ;
#57016=CARTESIAN_POINT ( 'NONE',  ( -81.90141697262173182, -25.33009845126374771, 4.495758016894969344 ) ) ;
#57017=CARTESIAN_POINT ( 'NONE',  ( -69.38261850605717029, -25.24515179376014018, 5.944601484458109653 ) ) ;
#57019=CARTESIAN_POINT ( 'NONE',  ( -18.79874323561663729, 6.599581278811135654, 11.49999999999998934 ) ) ;
#57021=CARTESIAN_POINT ( 'NONE',  ( -75.64825312942650726, -23.85049219812685806, 10.88485053497527488 ) ) ;
#57022=CARTESIAN_POINT ( 'NONE',  ( -18.60049703728633474, -6.982253431394513932, -1.500000000000002220 ) ) ;
#57024=CARTESIAN_POINT ( 'NONE',  ( -56.48830708450546467, -24.65952944569304250, 1.056160979905696795 ) ) ;
#57027=CARTESIAN_POINT ( 'NONE',  ( -44.62287095715004881, -29.50250786944525672, 11.44777988621624232 ) ) ;
#57028=CARTESIAN_POINT ( 'NONE',  ( -29.52287095715006870, -24.43005622135203936, 9.387565107222346938 ) ) ;
#57030=CARTESIAN_POINT ( 'NONE',  ( -20.13249939377427111, -5.111880259578561514, 11.49999999999999645 ) ) ;
#57034=CARTESIAN_POINT ( 'NONE',  ( 4.459850365305920938, 22.40387240153798487, 11.49999999999999645 ) ) ;
#57035=ORIENTED_EDGE ( 'NONE', *, *, #88086, .T. ) ;
#57037=EDGE_CURVE ( 'NONE', #49598, #234, #83292, .T. ) ;
#57038=DIRECTION ( 'NONE',  ( -3.773278334453080206E-23, 0.9999999999976377785, 2.173523156925979975E-06 ) ) ;
#57040=CARTESIAN_POINT ( 'NONE',  ( -17.47620107869530770, 10.18187089365592612, -1.500000000000002220 ) ) ;
#57043=B_SPLINE_CURVE_WITH_KNOTS ( 'NONE', 3,
 ( #94310, #11082, #49658, #2480 ),
 .UNSPECIFIED., .F., .F.,
 ( 4, 4 ),
 ( 0.000000000000000000, 1.000000000000000000 ),
 .UNSPECIFIED. ) ;
#57045=ADVANCED_FACE ( 'NONE', ( #40912 ), #80471, .T. ) ;
#57046=CARTESIAN_POINT ( 'NONE',  ( -50.52287095715006160, -23.48786465467241058, 11.44779295918255002 ) ) ;
#57047=VERTEX_POINT ( 'NONE', #50524 ) ;
#57048=CARTESIAN_POINT ( 'NONE',  ( -40.58953762381673158, -23.48786465467240347, 11.44779295918255180 ) ) ;
#57049=CARTESIAN_POINT ( 'NONE',  ( -84.52287095715006160, -24.64965694238406613, 8.947790433994198267 ) ) ;
#57050=CARTESIAN_POINT ( 'NONE',  ( 5.980626343040887249, -19.09133569553460319, -1.500000000000002220 ) ) ;
#57051=CARTESIAN_POINT ( 'NONE',  ( -20.70934228997045068, 3.328930095467914185, 11.49999999999999645 ) ) ;
#57053=CARTESIAN_POINT ( 'NONE',  ( -113.5228709571500616, -23.47593901973090524, -1.443836447538996204 ) ) ;
#57054=CARTESIAN_POINT ( 'NONE',  ( 14.91618686576236108, -16.25093855066790738, -1.500000000000002220 ) ) ;
#57055=B_SPLINE_CURVE_WITH_KNOTS ( 'NONE', 3,
 ( #78401, #85018, #60713, #22606 ),
 .UNSPECIFIED., .F., .F.,
 ( 4, 4 ),
 ( 0.7493128662882344582, 0.7503136133289997067 ),
 .UNSPECIFIED. ) ;
#57056=CARTESIAN_POINT ( 'NONE',  ( -40.20932372006943467, -25.31589326768515491, 5.067940297764987889 ) ) ;
#57057=ORIENTED_EDGE ( 'NONE', *, *, #49507, .T. ) ;
#57059=CARTESIAN_POINT ( 'NONE',  ( -47.58953762381671737, -24.65952944569304250, 1.056160979905693686 ) ) ;
#57062=VERTEX_POINT ( 'NONE', #96207 ) ;
#57064=ORIENTED_EDGE ( 'NONE', *, *, #43144, .F. ) ;
#57069=CARTESIAN_POINT ( 'NONE',  ( -18.81443736134900035, 8.205417114561466718, -1.500000000000002220 ) ) ;
#57070=ORIENTED_EDGE ( 'NONE', *, *, #76010, .T. ) ;
#57073=CARTESIAN_POINT ( 'NONE',  ( -96.58953762381671027, -24.66019654487199730, 8.947790411086126383 ) ) ;
#57074=CARTESIAN_POINT ( 'NONE',  ( -10.99827004860668822, -19.42154297629913628, -1.500000000000002220 ) ) ;
#57076=CARTESIAN_POINT ( 'NONE',  ( -32.07722060962682775, -25.12026506542016335, 2.831122744435439209 ) ) ;
#57077=EDGE_CURVE ( 'NONE', #26881, #55585, #63924, .T. ) ;
#57078=ORIENTED_EDGE ( 'NONE', *, *, #56668, .T. ) ;
#57079=CARTESIAN_POINT ( 'NONE',  ( -86.62287095715004170, -29.50250243563736774, 8.947779886222139822 ) ) ;
#57080=CARTESIAN_POINT ( 'NONE',  ( -65.58953762381672448, -24.99132157543084176, 2.256160258750496084 ) ) ;
#57082=CARTESIAN_POINT ( 'NONE',  ( -16.98601802344612111, -12.12340321765213069, -1.500000000000002220 ) ) ;
#57083=AXIS2_PLACEMENT_3D ( 'NONE', #88845, #34553, #57409 ) ;
#57085=CARTESIAN_POINT ( 'NONE',  ( -116.5228709571500474, -24.34917612407043563, 0.1852690917480298016 ) ) ;
#57089=CARTESIAN_POINT ( 'NONE',  ( -32.50560601784287229, -24.86181184613565165, 1.747789954104514987 ) ) ;
#57090=CARTESIAN_POINT ( 'NONE',  ( 20.41947327098772647, -5.118016103960565388, -1.500000000000002220 ) ) ;
#57091=VERTEX_POINT ( 'NONE', #42434 ) ;
#57093=CARTESIAN_POINT ( 'NONE',  ( -53.52287095715006870, -24.64965694238574656, 8.947790433994203596 ) ) ;
#57094=CARTESIAN_POINT ( 'NONE',  ( -120.5530840431339925, -24.73531770709095312, 8.716586749053508498 ) ) ;
#57095=CARTESIAN_POINT ( 'NONE',  ( -101.9401486745561272, -25.03152172299557066, 6.289339500554307349 ) ) ;
#57096=FACE_OUTER_BOUND ( 'NONE', #73528, .T. ) ;
#57097=CARTESIAN_POINT ( 'NONE',  ( 9.217229664113554932, 19.63635308506117383, -1.500000000000002220 ) ) ;
#57098=CARTESIAN_POINT ( 'NONE',  ( -80.72310326078591913, -25.12224386673238286, 7.076933481137675841 ) ) ;
#57099=CARTESIAN_POINT ( 'NONE',  ( -10.38793682863964563, 19.71736701935523683, 11.49999999999999645 ) ) ;
#57105=CARTESIAN_POINT ( 'NONE',  ( -120.5228709571500616, -29.50247984919015209, -1.443849546365046699 ) ) ;
#57110=CARTESIAN_POINT ( 'NONE',  ( -47.52287095715006160, -24.64965694238406613, 8.947790433994203596 ) ) ;
#57111=EDGE_CURVE ( 'NONE', #71528, #65697, #66253, .T. ) ;
#57114=EDGE_LOOP ( 'NONE', ( #97750, #80135, #11970, #79497 ) ) ;
#57115=CARTESIAN_POINT ( 'NONE',  ( -130.5728709571500588, -24.88728116469533447, 1.475554971460544262 ) ) ;
#57116=CARTESIAN_POINT ( 'NONE',  ( 11.64234319522276095, -19.14997049866658330, -1.500000000000002220 ) ) ;
#57119=CARTESIAN_POINT ( 'NONE',  ( -101.5221917529393210, -23.48786465467241413, 11.44779295918254469 ) ) ;
#57120=LINE ( 'NONE', #8921, #42544 ) ;
#57125=CARTESIAN_POINT ( 'NONE',  ( -130.5728709571500588, -24.37907397113050223, 9.703205396196697308 ) ) ;
#57126=CARTESIAN_POINT ( 'NONE',  ( -14.26233628608129855, 13.40890954296891024, 11.49999999999998934 ) ) ;
#57127=B_SPLINE_SURFACE_WITH_KNOTS ( 'NONE', 3, 1, ( 
 ( #8721, #85838 ),
 ( #84829, #69621 ),
 ( #54898, #39657 ),
 ( #63021, #93944 ),
 ( #85326, #16321 ),
 ( #31546, #15816 ),
 ( #46779, #1614 ),
 ( #102, #86341 ),
 ( #77705, #31040 ),
 ( #71122, #70615 ),
 ( #7708, #62007 ),
 ( #92437, #93436 ),
 ( #94450, #16824 ),
 ( #23931, #24932 ),
 ( #70114, #22904 ),
 ( #24432, #53897 ),
 ( #62508, #8218 ),
 ( #47284, #78211 ),
 ( #39157, #1106 ) ),
 .UNSPECIFIED., .F., .F., .F.,
 ( 4, 1, 1, 1, 1, 1, 1, 1, 1, 1, 1, 1, 1, 1, 1, 1, 4 ),
 ( 2, 2 ),
 ( 0.000000000000000000, 0.06196540068706264670, 0.1221219056382944895, 0.1809884968498423341, 0.2399332164519021315, 0.2999058311065245230, 0.3599888474769850633, 0.4217757417416482246, 0.4865758264211246797, 0.5515348046197418030, 0.6150175427599803291, 0.6772586166616564318, 0.7397299623627153764, 0.8030501026629509598, 0.8664951320156968340, 0.9319734741771505959, 1.000000000000000000 ),
 ( 0.000000000000000000, 1.000000000000000000 ),
 .UNSPECIFIED. ) ;
#57128=CARTESIAN_POINT ( 'NONE',  ( -50.12325739912953537, -25.31187256814138919, 4.701396598943802019 ) ) ;
#57130=EDGE_CURVE ( 'NONE', #57364, #93093, #73862, .T. ) ;
#57131=CARTESIAN_POINT ( 'NONE',  ( 4.075586527997184128, 21.15050231453075824, -1.500000000000002220 ) ) ;
#57133=CARTESIAN_POINT ( 'NONE',  ( -119.5228709571500758, -23.47596703998600631, 11.44779298504227860 ) ) ;
#57134=CARTESIAN_POINT ( 'NONE',  ( -107.6228709571500701, -23.48783264082479150, -1.443836473390060382 ) ) ;
#57136=CARTESIAN_POINT ( 'NONE',  ( -4.681240387505234857, -22.43558246840685300, -1.500000000000002220 ) ) ;
#57137=AXIS2_PLACEMENT_3D ( 'NONE', #14029, #99272, #4579 ) ;
#57139=CARTESIAN_POINT ( 'NONE',  ( -93.62287095715007013, -23.73907113216991860, -1.053371485793227924 ) ) ;
#57141=CARTESIAN_POINT ( 'NONE',  ( -16.95507112718987486, -10.73317591066004084, 11.49999999999999645 ) ) ;
#57143=CARTESIAN_POINT ( 'NONE',  ( -32.64292555811511676, -24.15620529776627734, 10.23563542870661358 ) ) ;
#57145=PLANE ( 'NONE',  #3485 ) ;
#57146=CARTESIAN_POINT ( 'NONE',  ( -96.52287095715006160, -23.47596703998600631, 11.44779298504228215 ) ) ;
#57148=CARTESIAN_POINT ( 'NONE',  ( 19.84127317031322946, -0.4231496731191971561, -1.500000000000002220 ) ) ;
#57151=CARTESIAN_POINT ( 'NONE',  ( -16.88869819569221065, 10.18974688345344148, -1.500000000000002220 ) ) ;
#57152=FACE_OUTER_BOUND ( 'NONE', #32956, .T. ) ;
#57156=VECTOR ( 'NONE', #80961, 1000.000000000000114 ) ;
#57158=CARTESIAN_POINT ( 'NONE',  ( -111.5228709571500616, -23.73907113216990439, -1.053371485793247242 ) ) ;
#57159=CARTESIAN_POINT ( 'NONE',  ( -19.88974639711211623, -5.441847772814488948, 11.49999999999999645 ) ) ;
#57160=ADVANCED_FACE ( 'NONE', ( #51031 ), #75342, .F. ) ;
#57162=CARTESIAN_POINT ( 'NONE',  ( 14.74224262856723833, 17.19160420931263999, 11.49999999999999645 ) ) ;
#57164=CARTESIAN_POINT ( 'NONE',  ( -102.5895376238167103, -24.65952944569304606, 1.056160979905698571 ) ) ;
#57165=CARTESIAN_POINT ( 'NONE',  ( -97.62752529066908380, -24.34968618360934300, 0.1864209137778856384 ) ) ;
#57166=CARTESIAN_POINT ( 'NONE',  ( -27.61431623538372548, -24.77705460396850512, 2.278732773682637269 ) ) ;
#57167=CARTESIAN_POINT ( 'NONE',  ( -127.5228709571500900, -23.72773821059536914, 11.05748984161097326 ) ) ;
#57169=LINE ( 'NONE', #17078, #77160 ) ;
#57170=EDGE_CURVE ( 'NONE', #6520, #51171, #14274, .T. ) ;
#57173=CARTESIAN_POINT ( 'NONE',  ( -79.34938298551102775, -25.31596414855141930, 5.853656268619368497 ) ) ;
#57174=CARTESIAN_POINT ( 'NONE',  ( -18.62658236799572720, 13.20813282334384553, -1.500000000000002220 ) ) ;
#57176=EDGE_CURVE ( 'NONE', #69024, #19418, #21056, .T. ) ;
#57177=CARTESIAN_POINT ( 'NONE',  ( -96.50665353833102245, -24.65952944569305316, 1.056160979905706121 ) ) ;
#57178=CARTESIAN_POINT ( 'NONE',  ( -82.59187514100537442, -24.15620529776628089, 10.23563542870660825 ) ) ;
#57180=CARTESIAN_POINT ( 'NONE',  ( -14.31525571501011207, 17.33968770572689166, 11.49999999999999645 ) ) ;
#57181=ORIENTED_EDGE ( 'NONE', *, *, #68881, .T. ) ;
#57183=CARTESIAN_POINT ( 'NONE',  ( -20.58003014649542095, 7.718188279156099618, 11.49999999999998934 ) ) ;
#57185=CARTESIAN_POINT ( 'NONE',  ( -111.5955121331480910, -23.48783264082477729, -1.443836473390087249 ) ) ;
#57186=DIRECTION ( 'NONE',  ( 0.000000000000000000, -2.173523156925980399E-06, 0.9999999999976378895 ) ) ;
#57188=ORIENTED_EDGE ( 'NONE', *, *, #15865, .T. ) ;
#57190=CARTESIAN_POINT ( 'NONE',  ( -107.5228709571500900, -24.50321055353805377, 9.387540953477515160 ) ) ;
#57191=ORIENTED_EDGE ( 'NONE', *, *, #48887, .F. ) ;
#57192=CARTESIAN_POINT ( 'NONE',  ( -54.63280671366005947, -24.35071581493543391, 9.817618358456034144 ) ) ;
#57193=CARTESIAN_POINT ( 'NONE',  ( 19.38413035786728145, -6.671778716439519030, 11.49999999999998934 ) ) ;
#57194=EDGE_LOOP ( 'NONE', ( #69753, #90734, #6646, #2152 ) ) ;
#57195=ORIENTED_EDGE ( 'NONE', *, *, #37785, .T. ) ;
#57197=ORIENTED_EDGE ( 'NONE', *, *, #95007, .F. ) ;
#57199=CARTESIAN_POINT ( 'NONE',  ( 22.28998074345494729, -6.091270044117925053, 11.49999999999998934 ) ) ;
#57200=CARTESIAN_POINT ( 'NONE',  ( -41.52287095715008292, -24.35013146730203815, 9.818937971375104823 ) ) ;
#57201=CARTESIAN_POINT ( 'NONE',  ( -9.871001836803966256, -17.81128643866572148, -1.500000000000002220 ) ) ;
#57202=ORIENTED_EDGE ( 'NONE', *, *, #1444, .T. ) ;
#57203=CARTESIAN_POINT ( 'NONE',  ( -71.18365115483554462, -25.08868281807281519, 7.289250223163644016 ) ) ;
#57204=CARTESIAN_POINT ( 'NONE',  ( -29.53717958776107366, -24.26755322398480885, 9.817618405055078767 ) ) ;
#57205=B_SPLINE_CURVE_WITH_KNOTS ( 'NONE', 3,
 ( #80404, #2796, #87012, #57089 ),
 .UNSPECIFIED., .F., .F.,
 ( 4, 4 ),
 ( 3.169701060731301374E-09, 0.001213954044779386957 ),
 .UNSPECIFIED. ) ;
#57206=CARTESIAN_POINT ( 'NONE',  ( -40.52287095715006870, -23.47596703998600631, 11.44779298504229281 ) ) ;
#57207=CARTESIAN_POINT ( 'NONE',  ( -71.03336120160147971, -25.03149811950544645, 7.389033691368496193 ) ) ;
#57209=CARTESIAN_POINT ( 'NONE',  ( -28.81395509834238311, -25.21531791893868402, 2.889655623812062313 ) ) ;
#57210=CARTESIAN_POINT ( 'NONE',  ( -49.10641598061040725, -25.26385650276297667, 4.048599411326989639 ) ) ;
#57211=B_SPLINE_CURVE_WITH_KNOTS ( 'NONE', 3,
 ( #84174, #22762, #14664, #84676 ),
 .UNSPECIFIED., .F., .F.,
 ( 4, 4 ),
 ( 0.000000000000000000, 0.0001000000000000028644 ),
 .UNSPECIFIED. ) ;
#57213=CARTESIAN_POINT ( 'NONE',  ( -19.91680486407696904, 5.911688619927280008, 11.49999999999998934 ) ) ;
#57215=CARTESIAN_POINT ( 'NONE',  ( -125.6246441017137840, -24.40034930558991633, 0.3402023900116222244 ) ) ;
#57218=B_SPLINE_SURFACE_WITH_KNOTS ( 'NONE', 3, 3, ( 
 ( #49064, #370, #31317, #876 ),
 ( #62798, #62287, #94717, #93712 ),
 ( #55179, #39934, #70896, #1387 ),
 ( #32322, #63294, #56180, #94213 ),
 ( #32825, #87105, #34330, #81997 ),
 ( #82486, #28208, #19587, #65798 ),
 ( #35824, #10987, #95723, #73394 ) ),
 .UNSPECIFIED., .F., .F., .F.,
 ( 4, 3, 4 ),
 ( 4, 4 ),
 ( 0.7945040050992238090, 0.8970133687736503436, 0.9995227324480768782 ),
 ( 0.8597124620935061579, 0.8611220869707849612 ),
 .UNSPECIFIED. ) ;
#57219=CARTESIAN_POINT ( 'NONE',  ( -122.6228709571500417, -24.64965695001469115, 8.947790433994175174 ) ) ;
#57220=CARTESIAN_POINT ( 'NONE',  ( -51.82604781446892162, -25.28888632563197802, 5.652223579025216438 ) ) ;
#57221=ORIENTED_EDGE ( 'NONE', *, *, #99358, .T. ) ;
#57222=ORIENTED_EDGE ( 'NONE', *, *, #27010, .T. ) ;
#57225=FACE_OUTER_BOUND ( 'NONE', #7578, .T. ) ;
#57226=CARTESIAN_POINT ( 'NONE',  ( -13.58966412916292299, 17.40808962483262690, 11.49999999999999645 ) ) ;
#57228=CARTESIAN_POINT ( 'NONE',  ( -48.88077023010853850, -25.24573983383035269, 6.307065433768737961 ) ) ;
#57229=VECTOR ( 'NONE', #13867, 1000.000000000000114 ) ;
#57230=CARTESIAN_POINT ( 'NONE',  ( -14.16962031475959272, 17.58799634409329471, -1.500000000000002220 ) ) ;
#57231=CARTESIAN_POINT ( 'NONE',  ( -129.5228709571500758, -23.47593901973090524, -1.443836447538996204 ) ) ;
#57232=ORIENTED_EDGE ( 'NONE', *, *, #17255, .T. ) ;
#57236=CARTESIAN_POINT ( 'NONE',  ( -94.55620429048339304, -24.64898659630529210, 1.056161002820827699 ) ) ;
#57238=CARTESIAN_POINT ( 'NONE',  ( -18.51692787870624102, -10.26217664800131502, -1.500000000000002220 ) ) ;
#57241=CARTESIAN_POINT ( 'NONE',  ( -69.62287095715005592, -29.50250786944525672, 11.44777988621623699 ) ) ;
#57242=CARTESIAN_POINT ( 'NONE',  ( 5.796264663052079769, -21.44337444023769379, -1.500000000000002220 ) ) ;
#57245=B_SPLINE_CURVE_WITH_KNOTS ( 'NONE', 3,
 ( #31644, #85939, #84435, #62613 ),
 .UNSPECIFIED., .F., .F.,
 ( 4, 4 ),
 ( 0.4701216268238749829, 0.4791280580959905167 ),
 .UNSPECIFIED. ) ;
#57250=EDGE_CURVE ( 'NONE', #68269, #40045, #90085, .T. ) ;
#57251=EDGE_CURVE ( 'NONE', #35157, #56064, #55455, .T. ) ;
#57252=CARTESIAN_POINT ( 'NONE',  ( -36.47910878338743856, -24.66019654487199730, 8.947790411086113949 ) ) ;
#57255=CARTESIAN_POINT ( 'NONE',  ( 19.46547125265945155, -1.073068822128883104, -1.500000000000002220 ) ) ;
#57257=CARTESIAN_POINT ( 'NONE',  ( 20.36625868517733196, 6.724766957447481097, 11.49999999999998934 ) ) ;
#57261=B_SPLINE_CURVE_WITH_KNOTS ( 'NONE', 3,
 ( #46340, #99605, #30610, #52966 ),
 .UNSPECIFIED., .F., .F.,
 ( 4, 4 ),
 ( 0.000000000000000000, 9.999999999998897304E-05 ),
 .UNSPECIFIED. ) ;
#57262=CARTESIAN_POINT ( 'NONE',  ( 21.04450177026006230, 8.645109164175620364, -1.500000000000002220 ) ) ;
#57265=CARTESIAN_POINT ( 'NONE',  ( -102.6251342045818120, -24.51314013834316086, 0.6176544820404232805 ) ) ;
#57266=CARTESIAN_POINT ( 'NONE',  ( -101.6228709571500559, -24.66019654487199730, 8.947790411086121054 ) ) ;
#57267=CARTESIAN_POINT ( 'NONE',  ( -19.91179686852411734, 0.6080443046932394457, 11.49999999999999645 ) ) ;
#57268=CARTESIAN_POINT ( 'NONE',  ( -100.4498239493576648, -29.50249942614374277, 7.563164501610023294 ) ) ;
#57270=CARTESIAN_POINT ( 'NONE',  ( -39.59379972882672405, -24.15620529776628089, 10.23563542870661180 ) ) ;
#57271=CARTESIAN_POINT ( 'NONE',  ( -48.60673731413511689, -23.73766607897670866, -1.055555164236436250 ) ) ;
#57275=CARTESIAN_POINT ( 'NONE',  ( -62.62287095715004881, -23.47596703998600276, 11.44779298504227505 ) ) ;
#57276=CARTESIAN_POINT ( 'NONE',  ( 19.61570337458852364, 9.273991169892711994, -1.500000000000002220 ) ) ;
#57277=CARTESIAN_POINT ( 'NONE',  ( -84.52287095715006160, -23.48786465467241769, 11.44779295918254469 ) ) ;
#57278=CARTESIAN_POINT ( 'NONE',  ( -1.081029368968937421, 19.50181592447522050, -1.500000000000002220 ) ) ;
#57283=LINE ( 'NONE', #49656, #54853 ) ;
#57284=CARTESIAN_POINT ( 'NONE',  ( -11.47117155886032158, -16.94740806926979815, 11.49999999999999645 ) ) ;
#57285=FACE_OUTER_BOUND ( 'NONE', #39210, .T. ) ;
#57286=CARTESIAN_POINT ( 'NONE',  ( -39.62287095715005592, -23.47596703998600276, 11.44779298504227505 ) ) ;
#57289=CARTESIAN_POINT ( 'NONE',  ( -66.52287095715006160, -24.64898659630528854, 1.056161002820824368 ) ) ;
#57291=DIRECTION ( 'NONE',  ( 0.000000000000000000, 0.9999999999976377785, 2.173523156925979128E-06 ) ) ;
#57292=CARTESIAN_POINT ( 'NONE',  ( -67.55620429048342146, -23.47596703998600276, 11.44779298504227505 ) ) ;
#57293=VECTOR ( 'NONE', #15636, 1000.000000000000114 ) ;
#57294=EDGE_LOOP ( 'NONE', ( #92710, #74416, #17498, #15024 ) ) ;
#57296=EDGE_CURVE ( 'NONE', #90027, #37337, #31170, .T. ) ;
#57297=CARTESIAN_POINT ( 'NONE',  ( -19.99251892732797486, -11.32171818645973538, 11.49999999999999645 ) ) ;
#57298=CARTESIAN_POINT ( 'NONE',  ( 22.46337926046256328, 3.617889471270266277, 11.49999999999998934 ) ) ;
#57299=CARTESIAN_POINT ( 'NONE',  ( -71.18885426527195648, -25.09962176569951708, 7.285300137760615691 ) ) ;
#57301=DIRECTION ( 'NONE',  ( -3.773278334453080206E-23, 0.9999999999976377785, 2.173523156925979975E-06 ) ) ;
#57302=CARTESIAN_POINT ( 'NONE',  ( -90.50599089165145017, -24.52300882791529801, 0.6510814631126391472 ) ) ;
#57304=CARTESIAN_POINT ( 'NONE',  ( -69.69184276925987831, -25.16776650702847817, 6.893752584519336146 ) ) ;
#57306=CARTESIAN_POINT ( 'NONE',  ( -16.30586240431254197, 14.59307310709210626, 11.49999999999998934 ) ) ;
#57307=CARTESIAN_POINT ( 'NONE',  ( -69.62363805984224996, -24.66019654487199375, 8.947790411086119278 ) ) ;
#57308=CARTESIAN_POINT ( 'NONE',  ( -115.6228709571500701, -24.83602698348160942, 1.605859176311268621 ) ) ;
#57310=CARTESIAN_POINT ( 'NONE',  ( -58.49789633566423674, -24.34968618360933945, 0.1864209137778795045 ) ) ;
#57312=CARTESIAN_POINT ( 'NONE',  ( -10.01004151551622456, -17.79114453763541093, -1.500000000000002220 ) ) ;
#57313=ORIENTED_EDGE ( 'NONE', *, *, #26561, .F. ) ;
#57315=CARTESIAN_POINT ( 'NONE',  ( -19.18584950847915493, -12.73052202388904952, -1.500000000000002220 ) ) ;
#57316=CARTESIAN_POINT ( 'NONE',  ( -95.62287095715005592, -29.50249982740957577, 7.747779886224967605 ) ) ;
#57319=CARTESIAN_POINT ( 'NONE',  ( -43.62287095715004881, -29.50248528299804818, 1.056150453629031594 ) ) ;
#57320=CARTESIAN_POINT ( 'NONE',  ( -101.1944152955115044, -25.16311295231453826, 6.858246048749960799 ) ) ;
#57321=VECTOR ( 'NONE', #86085, 1000.000000000000114 ) ;
#57323=CARTESIAN_POINT ( 'NONE',  ( -53.58245071975559881, -24.51419770103157347, 9.386484678747180510 ) ) ;
#57324=CARTESIAN_POINT ( 'NONE',  ( 21.20698605602738951, -2.876969938318672870, 11.49999999999999645 ) ) ;
#57326=ORIENTED_EDGE ( 'NONE', *, *, #78074, .F. ) ;
#57327=CARTESIAN_POINT ( 'NONE',  ( -9.187330254778467875, -20.22999604658808082, -1.500000000000002220 ) ) ;
#57328=CARTESIAN_POINT ( 'NONE',  ( 4.906390264955167169, 20.09725327650800608, -1.500000000000002220 ) ) ;
#57332=LINE ( 'NONE', #2531, #82651 ) ;
#57333=ORIENTED_EDGE ( 'NONE', *, *, #7154, .F. ) ;
#57334=CARTESIAN_POINT ( 'NONE',  ( 6.026637739148365548E-17, -29.50247984919009170, -1.443849575687677245 ) ) ;
#57335=VERTEX_POINT ( 'NONE', #12271 ) ;
#57336=AXIS2_PLACEMENT_3D ( 'NONE', #27024, #4190, #65611 ) ;
#57338=CARTESIAN_POINT ( 'NONE',  ( 18.03207908435136986, 10.65457695745678457, -1.500000000000002220 ) ) ;
#57339=CARTESIAN_POINT ( 'NONE',  ( -14.06357901826416068, -16.81340526219955933, 11.49999999999999645 ) ) ;
#57341=CARTESIAN_POINT ( 'NONE',  ( -37.62287095715006302, -23.96127896941632685, -0.6493128931037903673 ) ) ;
#57342=CARTESIAN_POINT ( 'NONE',  ( 21.68943130245101258, -6.005725296444199834, 11.49999999999998934 ) ) ;
#57343=CARTESIAN_POINT ( 'NONE',  ( -2.368302597431856782, 20.80102113048726409, 11.49999999999998934 ) ) ;
#57344=CARTESIAN_POINT ( 'NONE',  ( -26.09708441595108397, -24.97066806087577362, 5.016021429492140804 ) ) ;
#57346=CARTESIAN_POINT ( 'NONE',  ( -88.92287095715003886, -23.47593901973090169, -1.443836447538996870 ) ) ;
#57347=ORIENTED_EDGE ( 'NONE', *, *, #28566, .F. ) ;
#57350=CARTESIAN_POINT ( 'NONE',  ( -52.48647243912292026, -24.65952944569304606, 1.056160979905696351 ) ) ;
#57352=B_SPLINE_CURVE_WITH_KNOTS ( 'NONE', 3,
 ( #62321, #76512, #99843, #36967, #30351, #77013, #38469, #92743 ),
 .UNSPECIFIED., .F., .F.,
 ( 4, 2, 2, 4 ),
 ( -0.001240355328176662554, -0.0002398155169398004209, 0.0007607242942970617126, 0.002761803916770777523 ),
 .UNSPECIFIED. ) ;
#57353=CARTESIAN_POINT ( 'NONE',  ( 6.977786103627443559, 20.27319509581574408, -1.500000000000002220 ) ) ;
#57354=EDGE_LOOP ( 'NONE', ( #73300, #30223, #72907, #40946 ) ) ;
#57355=CARTESIAN_POINT ( 'NONE',  ( -26.09636659181000695, -24.95932275238217102, 4.940287574183225061 ) ) ;
#57356=CARTESIAN_POINT ( 'NONE',  ( -8.250207518706217158, 19.40231308534122689, -1.500000000000002220 ) ) ;
#57358=EDGE_CURVE ( 'NONE', #84227, #91131, #9432, .T. ) ;
#57360=CARTESIAN_POINT ( 'NONE',  ( -43.58953762381671027, -23.47596703998600276, 11.44779298504227505 ) ) ;
#57361=LINE ( 'NONE', #56860, #53989 ) ;
#57362=CARTESIAN_POINT ( 'NONE',  ( -109.3917100257398545, -25.30455905624913626, 4.480208735784438900 ) ) ;
#57363=CARTESIAN_POINT ( 'NONE',  ( -20.57682416348112397, 7.868404785394932155, -1.500000000000002220 ) ) ;
#57364=VERTEX_POINT ( 'NONE', #58971 ) ;
#57365=CARTESIAN_POINT ( 'NONE',  ( -65.59219749188024196, -24.40133493613049964, 9.663955038902800609 ) ) ;
#57366=AXIS2_PLACEMENT_3D ( 'NONE', #62521, #7214, #23424 ) ;
#57367=EDGE_CURVE ( 'NONE', #33030, #68434, #73606, .T. ) ;
#57369=CARTESIAN_POINT ( 'NONE',  ( -41.36802863981588274, -25.27956007679128803, 5.250400797641334272 ) ) ;
#57371=FACE_BOUND ( 'NONE', #63560, .T. ) ;
#57376=CARTESIAN_POINT ( 'NONE',  ( -0.3244385709253747585, -21.36021439428519386, 11.49999999999998934 ) ) ;
#57379=CARTESIAN_POINT ( 'NONE',  ( -91.62287095715004170, -23.47596703998600631, 11.44779298504227860 ) ) ;
#57381=CARTESIAN_POINT ( 'NONE',  ( -81.41755102971610825, -25.21105436082871876, 6.516612835075878962 ) ) ;
#57382=CARTESIAN_POINT ( 'NONE',  ( -19.71520456405594857, 11.01310763156902972, -1.500000000000002220 ) ) ;
#57383=CARTESIAN_POINT ( 'NONE',  ( -112.5895376238167245, -23.47593901973091235, -1.443836447538999312 ) ) ;
#57386=CARTESIAN_POINT ( 'NONE',  ( -79.54333787041024095, -24.51314013834316086, 0.6176544820404135105 ) ) ;
#57387=CARTESIAN_POINT ( 'NONE',  ( 19.69962056004252560, 1.334664424591413434, 11.49999999999999645 ) ) ;
#57388=CARTESIAN_POINT ( 'NONE',  ( -93.58953762381672448, -23.48786465467241769, 11.44779295918254114 ) ) ;
#57389=CARTESIAN_POINT ( 'NONE',  ( -67.54913149170559450, -24.15543982623906416, -0.2315651400026651485 ) ) ;
#57392=CARTESIAN_POINT ( 'NONE',  ( -39.52287095715006870, -24.65952944569304606, 1.056160979905691910 ) ) ;
#57393=LINE ( 'NONE', #47763, #79012 ) ;
#57394=CARTESIAN_POINT ( 'NONE',  ( -20.54952838774410750, 6.582847151591199264, -1.500000000000002220 ) ) ;
#57395=CARTESIAN_POINT ( 'NONE',  ( -71.55620429048339304, -23.47596703998600276, 11.44779298504227505 ) ) ;
#57397=B_SPLINE_CURVE_WITH_KNOTS ( 'NONE', 3,
 ( #99231, #43965, #98233, #91621, #12509, #28237 ),
 .UNSPECIFIED., .F., .F.,
 ( 4, 2, 4 ),
 ( 0.000000000000000000, 0.001381645795574012190, 0.002763291591148024379 ),
 .UNSPECIFIED. ) ;
#57398=CARTESIAN_POINT ( 'NONE',  ( -78.52287095715006160, -24.64898659630367916, 1.056161002820826145 ) ) ;
#57399=DIRECTION ( 'NONE',  ( -3.773278334453079030E-23, 0.9999999999976377785, 2.173523156925979128E-06 ) ) ;
#57400=CARTESIAN_POINT ( 'NONE',  ( -7.851535696030730982, 18.15458241006858131, -1.500000000000002220 ) ) ;
#57401=ORIENTED_EDGE ( 'NONE', *, *, #36633, .T. ) ;
#57402=CARTESIAN_POINT ( 'NONE',  ( -19.72078065558051208, -4.686549088087978099, 11.49999999999999645 ) ) ;
#57404=ORIENTED_EDGE ( 'NONE', *, *, #29102, .T. ) ;
#57405=CARTESIAN_POINT ( 'NONE',  ( -65.62287095715005592, -23.47596703998600631, 11.44779298504227683 ) ) ;
#57406=CARTESIAN_POINT ( 'NONE',  ( -99.72678786515000127, -25.29364544523226854, 4.454263737081315178 ) ) ;
#57408=CARTESIAN_POINT ( 'NONE',  ( -59.62287095715004881, -24.66019654487199020, 8.947790411086131712 ) ) ;
#57409=DIRECTION ( 'NONE',  ( -3.773278334444167608E-23, 1.000000000000000000, 0.000000000000000000 ) ) ;
#57410=CARTESIAN_POINT ( 'NONE',  ( -32.99388727629348494, -25.11010231571544082, 2.831122766524410750 ) ) ;
#57411=CARTESIAN_POINT ( 'NONE',  ( -4.446071851354966853, 19.53225066162704948, 11.49999999999998934 ) ) ;
#57413=ORIENTED_EDGE ( 'NONE', *, *, #78971, .F. ) ;
#57414=CARTESIAN_POINT ( 'NONE',  ( -32.62287095715005592, -24.51387760970722240, 9.387446482453418284 ) ) ;
#57415=DIRECTION ( 'NONE',  ( 0.000000000000000000, -2.173523156925979552E-06, 0.9999999999976378895 ) ) ;
#57416=CARTESIAN_POINT ( 'NONE',  ( -92.62287095715007013, -23.72773821059536559, 11.05748984161097681 ) ) ;
#57417=CARTESIAN_POINT ( 'NONE',  ( -119.6228709571500559, -29.50248528299804818, 1.056150453629045360 ) ) ;
#57419=EDGE_CURVE ( 'NONE', #53428, #79759, #28999, .T. ) ;
#57420=AXIS2_PLACEMENT_3D ( 'NONE', #53271, #16191, #76580 ) ;
#57422=ADVANCED_FACE ( 'NONE', ( #14762 ), #82786, .T. ) ;
#57423=CARTESIAN_POINT ( 'NONE',  ( -100.9368031010810398, -25.32724633150699844, 4.398074151685130495 ) ) ;
#57425=CARTESIAN_POINT ( 'NONE',  ( -16.58479117878708209, 11.75282063728064053, 11.49999999999998934 ) ) ;
#57427=CARTESIAN_POINT ( 'NONE',  ( -14.16064136294604303, -18.02537036913223290, 11.49999999999998934 ) ) ;
#57428=CARTESIAN_POINT ( 'NONE',  ( -32.66837636242299681, -23.48783264082477729, -1.443836473390076147 ) ) ;
#57430=CARTESIAN_POINT ( 'NONE',  ( -122.5228709571500616, -24.65952944569305316, 1.056160979905705899 ) ) ;
#57431=ORIENTED_EDGE ( 'NONE', *, *, #76576, .T. ) ;
#57432=DIRECTION ( 'NONE',  ( 0.000000000000000000, 0.9999999999976377785, 2.173523156925979128E-06 ) ) ;
#57434=CARTESIAN_POINT ( 'NONE',  ( -30.47287095715007155, -25.30769195857878984, 4.725583353285079724 ) ) ;
#57435=CARTESIAN_POINT ( 'NONE',  ( -0.1268723920767304558, 21.18662008908366445, 11.49999999999999645 ) ) ;
#57436=CARTESIAN_POINT ( 'NONE',  ( 18.07010470096111021, 12.80550835427630574, 11.49999999999998934 ) ) ;
#57437=B_SPLINE_CURVE_WITH_KNOTS ( 'NONE', 3,
 ( #78251, #40212, #8764, #70662, #40712, #32089 ),
 .UNSPECIFIED., .F., .F.,
 ( 4, 2, 4 ),
 ( 0.000000000000000000, 0.001380901958385391580, 0.002761803916770783161 ),
 .UNSPECIFIED. ) ;
#57439=CARTESIAN_POINT ( 'NONE',  ( -1.637206367458305500, 20.51943892441452633, -1.500000000000002220 ) ) ;
#57441=CARTESIAN_POINT ( 'NONE',  ( -41.51336541085899512, -23.73766607897670866, -1.055555164236442023 ) ) ;
#57443=CARTESIAN_POINT ( 'NONE',  ( -54.53713584333244313, -24.51314013834315020, 0.6176544820404069602 ) ) ;
#57444=CARTESIAN_POINT ( 'NONE',  ( -49.62287095715006302, -23.94994826722515313, -0.6494450866351706431 ) ) ;
#57447=EDGE_LOOP ( 'NONE', ( #78987, #65215, #39460, #56967 ) ) ;
#57449=CARTESIAN_POINT ( 'NONE',  ( -28.52988911114128356, -24.35371376620799211, 9.386484685950517104 ) ) ;
#57450=CARTESIAN_POINT ( 'NONE',  ( -102.5228709571500758, -29.50248528299804818, 1.056150453629042030 ) ) ;
#57451=CARTESIAN_POINT ( 'NONE',  ( -7.464567774302189207, 19.34240081622845153, -1.500000000000002220 ) ) ;
#57452=CARTESIAN_POINT ( 'NONE',  ( -15.31764660673900558, 15.41647822393392175, 11.49999999999999645 ) ) ;
#57456=CARTESIAN_POINT ( 'NONE',  ( -14.11974515630795501, -17.41659395067913962, 11.49999999999998934 ) ) ;
#57457=CARTESIAN_POINT ( 'NONE',  ( -92.92287095715002465, -23.47593901973090169, -1.443836447538996870 ) ) ;
#57459=EDGE_LOOP ( 'NONE', ( #74804, #99407, #2160, #31701 ) ) ;
#57461=CARTESIAN_POINT ( 'NONE',  ( -116.4728709548940628, -25.40673988423725405, 2.000950542041673774 ) ) ;
#57462=AXIS2_PLACEMENT_3D ( 'NONE', #31140, #61619, #22513 ) ;
#57464=B_SPLINE_CURVE_WITH_KNOTS ( 'NONE', 3,
 ( #90354, #68517, #29949, #46182, #45684, #14717 ),
 .UNSPECIFIED., .F., .F.,
 ( 4, 2, 4 ),
 ( 6.391158118972359742E-06, 0.001387004593080791133, 0.002767618028042609802 ),
 .UNSPECIFIED. ) ;
#57465=ORIENTED_EDGE ( 'NONE', *, *, #83784, .F. ) ;
#57466=CARTESIAN_POINT ( 'NONE',  ( -103.6228709571500417, -24.50216790748100237, 0.6166512839513710320 ) ) ;
#57467=ORIENTED_EDGE ( 'NONE', *, *, #12419, .T. ) ;
#57468=CARTESIAN_POINT ( 'NONE',  ( -6.410030533929251817, 20.24415959294862333, -1.500000000000002220 ) ) ;
#57469=B_SPLINE_CURVE_WITH_KNOTS ( 'NONE', 3,
 ( #84397, #83897, #83394, #61078, #39216, #6768 ),
 .UNSPECIFIED., .F., .F.,
 ( 4, 2, 4 ),
 ( 0.000000000000000000, 0.001380764517854760629, 0.002761529035709521258 ),
 .UNSPECIFIED. ) ;
#57471=CARTESIAN_POINT ( 'NONE',  ( -88.59843814960578356, -23.73766607897670511, -1.055555164236456678 ) ) ;
#57472=CARTESIAN_POINT ( 'NONE',  ( 19.92038474643397805, 8.973206291307779026, 11.49999999999998934 ) ) ;
#57473=CARTESIAN_POINT ( 'NONE',  ( -52.60591462248186190, -23.73791477778911840, 11.05961554403171299 ) ) ;
#57475=DIRECTION ( 'NONE',  ( -3.773278334444166432E-23, 1.000000000000000000, 0.000000000000000000 ) ) ;
#57476=CARTESIAN_POINT ( 'NONE',  ( 12.58402814888991372, -17.87355554032721372, -1.500000000000002220 ) ) ;
#57478=ORIENTED_EDGE ( 'NONE', *, *, #26231, .F. ) ;
#57481=ORIENTED_EDGE ( 'NONE', *, *, #79229, .T. ) ;
#57482=CARTESIAN_POINT ( 'NONE',  ( -30.64752034897746924, -23.47593901973090169, -1.443836447538997758 ) ) ;
#57484=EDGE_CURVE ( 'NONE', #81901, #87248, #67497, .T. ) ;
#57485=CARTESIAN_POINT ( 'NONE',  ( -40.02662638259540273, -25.26390949617024262, 6.217221587706935892 ) ) ;
#57487=CARTESIAN_POINT ( 'NONE',  ( -12.22836702412972087, 17.35733969022439993, -1.500000000000002220 ) ) ;
#57488=CARTESIAN_POINT ( 'NONE',  ( -37.62287095715005592, -29.50250243563736774, 8.947779886222148704 ) ) ;
#57489=ADVANCED_FACE ( 'NONE', ( #28504 ), #83932, .T. ) ;
#57491=AXIS2_PLACEMENT_3D ( 'NONE', #47285, #61516, #92438 ) ;
#57493=CARTESIAN_POINT ( 'NONE',  ( -68.60861524139340872, -23.48783264082476308, -1.443836473390094799 ) ) ;
#57494=CARTESIAN_POINT ( 'NONE',  ( -17.77321681866180469, -7.816401696202086136, 11.49999999999998934 ) ) ;
#57495=DIRECTION ( 'NONE',  ( -3.773278334453079030E-23, 0.9999999999976377785, 2.173523156925979128E-06 ) ) ;
#57496=ORIENTED_EDGE ( 'NONE', *, *, #9386, .F. ) ;
#57497=CARTESIAN_POINT ( 'NONE',  ( 13.97609912898263573, 13.72534901313461653, 11.49999999999999645 ) ) ;
#57499=CARTESIAN_POINT ( 'NONE',  ( -97.52287095715006160, -23.48786465467241769, 11.44779295918254114 ) ) ;
#57500=EDGE_CURVE ( 'NONE', #83990, #85754, #39623, .T. ) ;
#57503=CARTESIAN_POINT ( 'NONE',  ( -97.62287095715008434, -24.50216790748100237, 0.6166512839513762501 ) ) ;
#57504=CARTESIAN_POINT ( 'NONE',  ( -75.62287095715004170, -24.83602698348158810, 1.605859176311266179 ) ) ;
#57507=CARTESIAN_POINT ( 'NONE',  ( 8.085132396474181249, 17.94908993440701295, 11.49999999999998934 ) ) ;
#57508=B_SPLINE_CURVE_WITH_KNOTS ( 'NONE', 3,
 ( #49622, #11536, #11047, #72954 ),
 .UNSPECIFIED., .F., .F.,
 ( 4, 4 ),
 ( 0.000000000000000000, 1.000000000000000000 ),
 .UNSPECIFIED. ) ;
#57510=FACE_OUTER_BOUND ( 'NONE', #63029, .T. ) ;
#57511=PLANE ( 'NONE',  #43145 ) ;
#57517=CARTESIAN_POINT ( 'NONE',  ( -29.52287095715006160, -24.56627961951908645, 8.947790480023282811 ) ) ;
#57520=FACE_OUTER_BOUND ( 'NONE', #45575, .T. ) ;
#57521=CARTESIAN_POINT ( 'NONE',  ( 14.81759351585047391, 13.34335055255382052, 11.49999999999998934 ) ) ;
#57522=CARTESIAN_POINT ( 'NONE',  ( -100.6434263600250745, -25.19749065189113679, 3.311375407965762463 ) ) ;
#57523=CARTESIAN_POINT ( 'NONE',  ( -6.239078800006583769, 18.87631364486404806, -1.500000000000002220 ) ) ;
#57525=CARTESIAN_POINT ( 'NONE',  ( -29.52287095715006160, -24.56560739788454129, 1.056161319240904728 ) ) ;
#57527=LINE ( 'NONE', #57027, #7902 ) ;
#57531=CARTESIAN_POINT ( 'NONE',  ( 17.18838054715250152, -11.71887806637979779, 11.49999999999999645 ) ) ;
#57533=ADVANCED_FACE ( 'NONE', ( #61467 ), #43613, .T. ) ;
#57534=CARTESIAN_POINT ( 'NONE',  ( -50.91254006769597140, -25.20043120925951996, 3.405783117403155646 ) ) ;
#57536=CARTESIAN_POINT ( 'NONE',  ( 18.61037501828884189, -13.27421459584354579, 11.49999999999999645 ) ) ;
#57537=EDGE_LOOP ( 'NONE', ( #90753, #27716, #72716, #62709 ) ) ;
#57539=DIRECTION ( 'NONE',  ( 0.000000000000000000, -0.9999999999976377785, -2.173523156925979975E-06 ) ) ;
#57540=VERTEX_POINT ( 'NONE', #19752 ) ;
#57541=CARTESIAN_POINT ( 'NONE',  ( 16.63042848490962555, -11.55671354112608817, -1.500000000000002220 ) ) ;
#57543=DIRECTION ( 'NONE',  ( 0.000000000000000000, 0.9999999999976377785, 2.173523156925979128E-06 ) ) ;
#57546=CARTESIAN_POINT ( 'NONE',  ( -109.5228709571500616, -24.64965694238408034, 8.947790433994192938 ) ) ;
#57547=CARTESIAN_POINT ( 'NONE',  ( -30.53953689462962018, -23.47596701192223989, 11.43488133310209420 ) ) ;
#57548=CARTESIAN_POINT ( 'NONE',  ( -10.28607412905329532, -17.16720287211733975, -1.500000000000002220 ) ) ;
#57549=CARTESIAN_POINT ( 'NONE',  ( -9.798014431990228701, 18.61115389415964572, 11.49999999999999645 ) ) ;
#57552=CARTESIAN_POINT ( 'NONE',  ( 22.04941498731238525, 0.3350016526185666255, -1.500000000000002220 ) ) ;
#57559=CARTESIAN_POINT ( 'NONE',  ( -72.55911174566438149, -23.73766607897670156, -1.055555164236458454 ) ) ;
#57560=CARTESIAN_POINT ( 'NONE',  ( -31.49625347033022749, -24.15543982623907127, -0.2315651400026576545 ) ) ;
#57564=CARTESIAN_POINT ( 'NONE',  ( -100.4381051993576506, -25.27404630390602236, 2.832404461470396928 ) ) ;
#57565=CARTESIAN_POINT ( 'NONE',  ( -40.45829750704998418, -29.50249014687182836, 3.293933732389337621 ) ) ;
#57566=CARTESIAN_POINT ( 'NONE',  ( 19.76637988705548210, 5.604140092158477415, -1.500000000000002220 ) ) ;
#57569=CARTESIAN_POINT ( 'NONE',  ( -99.62287095715005592, -29.50247984919015209, -1.443849546365050029 ) ) ;
#57573=CARTESIAN_POINT ( 'NONE',  ( -22.12323335113916301, -3.008119206214963981, 11.49999999999998934 ) ) ;
#57577=VERTEX_POINT ( 'NONE', #10664 ) ;
#57580=CARTESIAN_POINT ( 'NONE',  ( 16.20321855003292555, -13.12800272717607619, 11.49999999999998934 ) ) ;
#57581=VERTEX_POINT ( 'NONE', #28374 ) ;
#57583=ORIENTED_EDGE ( 'NONE', *, *, #78006, .F. ) ;
#57585=CARTESIAN_POINT ( 'NONE',  ( -69.97463645619113493, -25.25935341538093581, 7.520861282928617442 ) ) ;
#57586=CARTESIAN_POINT ( 'NONE',  ( -17.90976863334866920, 11.11529090135583075, -1.500000000000002220 ) ) ;
#57587=ORIENTED_EDGE ( 'NONE', *, *, #15520, .F. ) ;
#57588=CARTESIAN_POINT ( 'NONE',  ( -114.6228709571500701, -23.95044443724992789, 10.65354141964649237 ) ) ;
#57589=CARTESIAN_POINT ( 'NONE',  ( -102.6228709571500133, -24.33927499327854704, 9.819080762295815390 ) ) ;
#57590=LINE ( 'NONE', #3800, #87019 ) ;
#57591=CARTESIAN_POINT ( 'NONE',  ( -101.9507253916653440, -25.03152160760679479, 6.236251142457633456 ) ) ;
#57592=CARTESIAN_POINT ( 'NONE',  ( -129.6228709571500701, -23.72773821059536559, 11.05748984161097503 ) ) ;
#57593=CARTESIAN_POINT ( 'NONE',  ( -14.16021466491576675, 16.42052772630311352, -1.500000000000002220 ) ) ;
#57594=CARTESIAN_POINT ( 'NONE',  ( -63.52287095715003318, -24.35013146730202749, 9.818937971375104823 ) ) ;
#57595=EDGE_CURVE ( 'NONE', #73714, #80473, #71087, .T. ) ;
#57596=CARTESIAN_POINT ( 'NONE',  ( 22.02009960291501045, 3.200778107580485532, 11.49999999999999645 ) ) ;
#57597=EDGE_LOOP ( 'NONE', ( #77881, #30883, #22318, #55840 ) ) ;
#57598=CARTESIAN_POINT ( 'NONE',  ( -72.62287095715005592, -24.66019654487199020, 8.947790411086131712 ) ) ;
#57600=CARTESIAN_POINT ( 'NONE',  ( -87.52287095715006160, -24.65952944569304606, 1.056160979905700570 ) ) ;
#57602=CARTESIAN_POINT ( 'NONE',  ( -41.52287095715005449, -24.66019654487198665, 8.947790411086121054 ) ) ;
#57603=VERTEX_POINT ( 'NONE', #72568 ) ;
#57604=ORIENTED_EDGE ( 'NONE', *, *, #14668, .F. ) ;
#57606=CARTESIAN_POINT ( 'NONE',  ( -57.58953762381672448, -23.47596703998600276, 11.44779298504227505 ) ) ;
#57608=CARTESIAN_POINT ( 'NONE',  ( -48.62287095715004881, -23.48783264082478439, -1.443836473390070596 ) ) ;
#57610=VERTEX_POINT ( 'NONE', #89785 ) ;
#57611=B_SPLINE_CURVE_WITH_KNOTS ( 'NONE', 3,
 ( #91770, #92772, #8549, #39503 ),
 .UNSPECIFIED., .F., .F.,
 ( 4, 4 ),
 ( 0.5191410469121615634, 0.5201417939529271450 ),
 .UNSPECIFIED. ) ;
#57613=CARTESIAN_POINT ( 'NONE',  ( 18.78116726530667080, 12.29669497462397842, -1.500000000000002220 ) ) ;
#57616=DIRECTION ( 'NONE',  ( -3.773278334453080206E-23, 0.9999999999976377785, 2.173523156925979975E-06 ) ) ;
#57617=PLANE ( 'NONE',  #49147 ) ;
#57619=CARTESIAN_POINT ( 'NONE',  ( -41.52287095715004739, -24.34917612407030063, 0.1852690917476942645 ) ) ;
#57620=CARTESIAN_POINT ( 'NONE',  ( -97.24791218068880028, -24.66513809378596989, 8.909134979017300893 ) ) ;
#57621=CARTESIAN_POINT ( 'NONE',  ( 17.47348308817029405, 8.859467055162037141, 11.49999999999998934 ) ) ;
#57624=CARTESIAN_POINT ( 'NONE',  ( -21.26083644630951142, -3.357327265692296780, -1.500000000000002220 ) ) ;
#57626=CARTESIAN_POINT ( 'NONE',  ( -70.94546041667526026, -25.12219101425611356, 6.902322780480511177 ) ) ;
#57627=CARTESIAN_POINT ( 'NONE',  ( -53.55620429048339304, -23.47596703998600276, 11.44779298504227505 ) ) ;
#57628=DIRECTION ( 'NONE',  ( -3.773278334453080206E-23, 0.9999999999976377785, 2.173523156925979975E-06 ) ) ;
#57629=CARTESIAN_POINT ( 'NONE',  ( -22.40196285382242536, -4.882868457752029379, -1.500000000000002220 ) ) ;
#57633=CARTESIAN_POINT ( 'NONE',  ( -53.54178288312186140, -24.34968618360933590, 0.1864209137778785885 ) ) ;
#57634=CARTESIAN_POINT ( 'NONE',  ( -19.74138705131307248, -3.616033589355840849, 11.49999999999999645 ) ) ;
#57635=DIRECTION ( 'NONE',  ( 0.000000000000000000, -0.9999999999976377785, -2.173523156925979975E-06 ) ) ;
#57637=AXIS2_PLACEMENT_3D ( 'NONE', #47864, #94524, #17405 ) ;
#57638=CARTESIAN_POINT ( 'NONE',  ( -121.6228709571500559, -23.47596703998600631, 11.44779298504227683 ) ) ;
#57639=DIRECTION ( 'NONE',  ( 1.000000000000000000, 3.773278334444166432E-23, 8.201307841325785021E-29 ) ) ;
#57641=CARTESIAN_POINT ( 'NONE',  ( -19.55781625546462976, 3.520333346782119843, 11.49999999999998934 ) ) ;
#57644=CARTESIAN_POINT ( 'NONE',  ( 16.13486940644654766, 11.28601765141728741, -1.500000000000002220 ) ) ;
#57646=CARTESIAN_POINT ( 'NONE',  ( -28.52287095715005805, -23.31185441368106126, 11.44779303854528685 ) ) ;
#57648=CARTESIAN_POINT ( 'NONE',  ( -103.5228709571500758, -24.64898659630367916, 1.056161002820829697 ) ) ;
#57650=CARTESIAN_POINT ( 'NONE',  ( 10.61356161029474521, 17.70173163822984819, 11.49999999999999645 ) ) ;
#57651=B_SPLINE_CURVE_WITH_KNOTS ( 'NONE', 3,
 ( #85168, #47125, #940, #78038, #8551, #31890, #93781, #24272, #86671, #46625 ),
 .UNSPECIFIED., .F., .F.,
 ( 4, 3, 3, 4 ),
 ( 0.000000000000000000, 0.0001187730049107982994, 0.0002375745643523147167, 0.0004748892031761914605 ),
 .UNSPECIFIED. ) ;
#57653=CARTESIAN_POINT ( 'NONE',  ( -17.75566480456612695, 14.03706703302619374, 11.49999999999999645 ) ) ;
#57655=ORIENTED_EDGE ( 'NONE', *, *, #60816, .T. ) ;
#57656=DIRECTION ( 'NONE',  ( -3.773278334453079030E-23, 0.9999999999976377785, 2.173523156925979128E-06 ) ) ;
#57657=CARTESIAN_POINT ( 'NONE',  ( -97.54592858886259421, -24.65952944569304606, 1.056160979905701680 ) ) ;
#57658=CARTESIAN_POINT ( 'NONE',  ( -127.5228709571500616, -23.95044443724993144, 10.65354141964648882 ) ) ;
#57660=B_SPLINE_CURVE_WITH_KNOTS ( 'NONE', 3,
 ( #31849, #10003, #33334, #87637, #19110, #35842 ),
 .UNSPECIFIED., .F., .F.,
 ( 4, 2, 4 ),
 ( 0.000000000000000000, 0.001380901958385387894, 0.002761803916770775788 ),
 .UNSPECIFIED. ) ;
#57662=CARTESIAN_POINT ( 'NONE',  ( -84.52287095715006160, -23.47596703998600631, 11.44779298504228571 ) ) ;
#57663=CARTESIAN_POINT ( 'NONE',  ( -5.953223121155255981, 22.05028593715628560, -1.500000000000002220 ) ) ;
#57664=CARTESIAN_POINT ( 'NONE',  ( -74.58127051957136189, -24.65952944569304606, 1.056160979905701680 ) ) ;
#57665=LINE ( 'NONE', #88608, #60951 ) ;
#57666=CARTESIAN_POINT ( 'NONE',  ( -82.51746163132445133, -23.73791477778912196, 11.05961554403170943 ) ) ;
#57667=AXIS2_PLACEMENT_3D ( 'NONE', #53903, #54401, #78216 ) ;
#57668=CARTESIAN_POINT ( 'NONE',  ( -8.346146134265904237, -20.86121191590761015, 11.49999999999999645 ) ) ;
#57669=ORIENTED_EDGE ( 'NONE', *, *, #79553, .F. ) ;
#57670=CARTESIAN_POINT ( 'NONE',  ( -43.49282179846755270, -24.34968618360933235, 0.1864209137778850833 ) ) ;
#57671=CARTESIAN_POINT ( 'NONE',  ( 6.372119535971386917, -21.01724095701019479, 11.49999999999998934 ) ) ;
#57672=EDGE_CURVE ( 'NONE', #16871, #62504, #97876, .T. ) ;
#57674=CARTESIAN_POINT ( 'NONE',  ( -29.20082839157102583, -25.21724613326715314, 5.852069579333174509 ) ) ;
#57677=CARTESIAN_POINT ( 'NONE',  ( -107.5228709571501042, -23.72773821059536914, 11.05748984161097503 ) ) ;
#57679=ADVANCED_FACE ( 'NONE', ( #65476 ), #59614, .T. ) ;
#57680=FACE_OUTER_BOUND ( 'NONE', #16137, .T. ) ;
#57681=CARTESIAN_POINT ( 'NONE',  ( -7.444040098415714013, -19.11467064512029879, -1.500000000000002220 ) ) ;
#57683=EDGE_LOOP ( 'NONE', ( #54535, #50340, #48822, #58707 ) ) ;
#57686=CARTESIAN_POINT ( 'NONE',  ( 17.26854690438276307, -15.35948741044508559, -1.500000000000002220 ) ) ;
#57687=CARTESIAN_POINT ( 'NONE',  ( -104.5551257925524453, -23.96169478059714208, 10.65365249895717525 ) ) ;
#57688=CARTESIAN_POINT ( 'NONE',  ( 20.12614038868121824, 2.982395457389826809, -1.500000000000002220 ) ) ;
#57690=CARTESIAN_POINT ( 'NONE',  ( -70.43580950499047333, -25.03347651911512273, 7.560241782797326060 ) ) ;
#57691=EDGE_CURVE ( 'NONE', #26881, #62407, #21747, .T. ) ;
#57692=CARTESIAN_POINT ( 'NONE',  ( -29.50320195067551765, -23.87474868272149209, 10.65365256123546978 ) ) ;
#57693=EDGE_CURVE ( 'NONE', #35458, #24252, #90484, .T. ) ;
#57694=CARTESIAN_POINT ( 'NONE',  ( -105.5930656460468953, -24.15503026093913164, -0.2815557561904565298 ) ) ;
#57697=CARTESIAN_POINT ( 'NONE',  ( -29.22054808153496808, -24.76881279543748704, 4.231944355383084222 ) ) ;
#57698=PLANE ( 'NONE',  #92819 ) ;
#57700=VERTEX_POINT ( 'NONE', #82662 ) ;
#57701=CARTESIAN_POINT ( 'NONE',  ( -20.73834036848188234, 1.213307192923735345, -1.500000000000002220 ) ) ;
#57702=ORIENTED_EDGE ( 'NONE', *, *, #19760, .F. ) ;
#57704=EDGE_LOOP ( 'NONE', ( #15, #36203, #57797, #24190 ) ) ;
#57706=CARTESIAN_POINT ( 'NONE',  ( -86.62287095715004170, -24.65952944569304606, 1.056160979905700348 ) ) ;
#57707=CARTESIAN_POINT ( 'NONE',  ( -107.6228709571500843, -23.72747288104441665, -1.053458166803660889 ) ) ;
#57709=EDGE_LOOP ( 'NONE', ( #37488, #96071, #70325, #48862 ) ) ;
#57711=CARTESIAN_POINT ( 'NONE',  ( -33.52287095715006160, -23.47596703998600631, 11.44779298504229459 ) ) ;
#57712=CARTESIAN_POINT ( 'NONE',  ( -116.6228709571500417, -23.48786465467241769, 11.44779295918253759 ) ) ;
#57713=VECTOR ( 'NONE', #58615, 1000.000000000000114 ) ;
#57714=CARTESIAN_POINT ( 'NONE',  ( -43.55308972817040569, -23.96169478059712787, 10.65365249895718769 ) ) ;
#57715=ADVANCED_FACE ( 'NONE', ( #36990 ), #30876, .T. ) ;
#57716=CARTESIAN_POINT ( 'NONE',  ( -22.03165466229905789, 1.424673820674137614, 11.49999999999999645 ) ) ;
#57718=VECTOR ( 'NONE', #19153, 1000.000000000000114 ) ;
#57719=FACE_OUTER_BOUND ( 'NONE', #91403, .T. ) ;
#57720=CARTESIAN_POINT ( 'NONE',  ( 11.26306171725914851, -19.60737681494043727, -1.500000000000002220 ) ) ;
#57721=VECTOR ( 'NONE', #233, 1000.000000000000114 ) ;
#57722=DIRECTION ( 'NONE',  ( -1.000000000000000000, -3.773278334444167608E-23, -8.201307833595939069E-29 ) ) ;
#57724=ORIENTED_EDGE ( 'NONE', *, *, #45987, .T. ) ;
#57726=EDGE_CURVE ( 'NONE', #70639, #73004, #80789, .T. ) ;
#57727=B_SPLINE_CURVE_WITH_KNOTS ( 'NONE', 3,
 ( #37853, #60708, #6900, #61703, #99726, #22112, #92131, #61211, #76888, #7389, #69300, #23105, #32732, #94127, #24611, #95139 ),
 .UNSPECIFIED., .F., .F.,
 ( 4, 2, 2, 2, 2, 2, 2, 4 ),
 ( 0.000000000000000000, 0.0002661357119279468509, 0.0005322714238558924008, 0.001064542847711783501, 0.001330678559639729159, 0.001596814271567674817, 0.001862949983495620476, 0.002129085695423566134 ),
 .UNSPECIFIED. ) ;
#57730=ORIENTED_EDGE ( 'NONE', *, *, #12309, .F. ) ;
#57731=CARTESIAN_POINT ( 'NONE',  ( -13.58512445790048417, 16.25115196636789250, -1.500000000000002220 ) ) ;
#57733=DIRECTION ( 'NONE',  ( 0.000000000000000000, 2.173523156925980399E-06, -0.9999999999976378895 ) ) ;
#57734=CARTESIAN_POINT ( 'NONE',  ( -13.27262489239681997, 17.90159134968837051, -1.500000000000002220 ) ) ;
#57735=FACE_OUTER_BOUND ( 'NONE', #48167, .T. ) ;
#57736=EDGE_CURVE ( 'NONE', #63440, #27806, #84155, .T. ) ;
#57738=CARTESIAN_POINT ( 'NONE',  ( -80.52287095715006160, -23.47596703998600631, 11.44779298504228571 ) ) ;
#57741=ADVANCED_FACE ( 'NONE', ( #46110 ), #35279, .T. ) ;
#57742=CARTESIAN_POINT ( 'NONE',  ( -41.51830428958714947, -25.18393819603653583, 3.285814443599428980 ) ) ;
#57743=CARTESIAN_POINT ( 'NONE',  ( -116.5895376238167387, -24.64898659630368627, 1.056161002820393158 ) ) ;
#57744=ADVANCED_FACE ( 'NONE', ( #86162 ), #88730, .T. ) ;
#57745=CARTESIAN_POINT ( 'NONE',  ( -13.24781383850973349, 14.34467480260970795, -1.500000000000002220 ) ) ;
#57746=CARTESIAN_POINT ( 'NONE',  ( 5.397486108853063236, 20.74927772461418485, 11.49999999999998934 ) ) ;
#57747=CARTESIAN_POINT ( 'NONE',  ( -27.40838375831408058, -24.57999501220895411, 1.648157300620804344 ) ) ;
#57749=CARTESIAN_POINT ( 'NONE',  ( -77.54284170824401201, -24.51314013834315375, 0.6176544820404117342 ) ) ;
#57750=CARTESIAN_POINT ( 'NONE',  ( 12.23086119556625206, 19.17791753167082192, -1.500000000000002220 ) ) ;
#57752=CARTESIAN_POINT ( 'NONE',  ( -102.5194659324134676, -23.73766607897671577, -1.055555164236430254 ) ) ;
#57753=CARTESIAN_POINT ( 'NONE',  ( -128.5228709571500758, -24.64898659630368627, 1.056161002820834804 ) ) ;
#57754=CARTESIAN_POINT ( 'NONE',  ( 2.927915493035635031, 19.71835975189664936, 11.49999999999999645 ) ) ;
#57755=CARTESIAN_POINT ( 'NONE',  ( -31.52287095715004739, -24.33832256527048088, 0.1851278514138553211 ) ) ;
#57756=CARTESIAN_POINT ( 'NONE',  ( -128.5228709571499905, -24.33927499327855770, 9.819080762295804732 ) ) ;
#57757=CARTESIAN_POINT ( 'NONE',  ( -48.55326441215460420, -23.96119346886881019, -0.6495511937831938143 ) ) ;
#57758=VERTEX_POINT ( 'NONE', #31881 ) ;
#57760=CARTESIAN_POINT ( 'NONE',  ( -31.82683686962402447, -24.87219037988794312, 1.747789950295619787 ) ) ;
#57761=CARTESIAN_POINT ( 'NONE',  ( 20.80172415560569021, 6.174449132348904357, -1.500000000000002220 ) ) ;
#57762=CARTESIAN_POINT ( 'NONE',  ( -56.50840713276495109, -23.96169478059713498, 10.65365249895718236 ) ) ;
#57763=CARTESIAN_POINT ( 'NONE',  ( -18.91883139384513157, -4.797682538509264738, -1.500000000000002220 ) ) ;
#57765=CARTESIAN_POINT ( 'NONE',  ( -55.65727299751092261, -23.85049219812685806, 10.88485053497527133 ) ) ;
#57769=CARTESIAN_POINT ( 'NONE',  ( 1.945971545120378288, -20.36639758168144709, 11.49999999999999645 ) ) ;
#57772=PLANE ( 'NONE',  #77216 ) ;
#57773=EDGE_LOOP ( 'NONE', ( #19478, #36262, #4259, #85905 ) ) ;
#57774=CARTESIAN_POINT ( 'NONE',  ( -52.92287095715005307, -23.47596703998600276, 11.44779298504227683 ) ) ;
#57778=AXIS2_PLACEMENT_3D ( 'NONE', #29859, #37479, #47971 ) ;
#57779=CARTESIAN_POINT ( 'NONE',  ( -55.62287095715005592, -23.47593901973091235, -1.443836447539007972 ) ) ;
#57780=VERTEX_POINT ( 'NONE', #33371 ) ;
#57782=AXIS2_PLACEMENT_3D ( 'NONE', #78574, #1484, #78075 ) ;
#57783=CARTESIAN_POINT ( 'NONE',  ( -3.987988226355533072, 22.59150145119509290, 11.49999999999999645 ) ) ;
#57784=CARTESIAN_POINT ( 'NONE',  ( 7.533951754900199305, 21.46025436219600024, 11.49999999999998934 ) ) ;
#57785=CARTESIAN_POINT ( 'NONE',  ( -70.79215990384717827, -25.05760859634946414, 7.494946593071406760 ) ) ;
#57786=FACE_OUTER_BOUND ( 'NONE', #95566, .T. ) ;
#57789=CARTESIAN_POINT ( 'NONE',  ( -69.34467035722860828, -25.24945287413907380, 6.270865876356967128 ) ) ;
#57790=CARTESIAN_POINT ( 'NONE',  ( -1.678574117887026373, -21.80011532881206548, -1.500000000000002220 ) ) ;
#57791=PLANE ( 'NONE',  #52691 ) ;
#57792=ADVANCED_FACE ( 'NONE', ( #80550 ), #44372, .F. ) ;
#57793=B_SPLINE_CURVE_WITH_KNOTS ( 'NONE', 3,
 ( #72451, #67218, #12898, #83409 ),
 .UNSPECIFIED., .F., .F.,
 ( 4, 4 ),
 ( 0.000000000000000000, 9.999999999998900014E-05 ),
 .UNSPECIFIED. ) ;
#57794=LINE ( 'NONE', #81618, #63889 ) ;
#57796=CARTESIAN_POINT ( 'NONE',  ( -58.57885350497856081, -24.65952944569304606, 1.056160979905697461 ) ) ;
#57797=ORIENTED_EDGE ( 'NONE', *, *, #16428, .T. ) ;
#57798=EDGE_CURVE ( 'NONE', #4648, #96462, #13396, .T. ) ;
#57799=CARTESIAN_POINT ( 'NONE',  ( -18.43012528856881715, -8.789534013050598560, -1.500000000000002220 ) ) ;
#57801=ORIENTED_EDGE ( 'NONE', *, *, #42828, .F. ) ;
#57802=ORIENTED_EDGE ( 'NONE', *, *, #75095, .T. ) ;
#57804=CARTESIAN_POINT ( 'NONE',  ( 13.47786528765806580, -18.65256936556403744, -1.500000000000002220 ) ) ;
#57805=PLANE ( 'NONE',  #27618 ) ;
#57806=CARTESIAN_POINT ( 'NONE',  ( 18.20877288740043198, -8.745817889818592761, -1.500000000000002220 ) ) ;
#57807=EDGE_CURVE ( 'NONE', #39894, #71598, #57793, .T. ) ;
#57810=CARTESIAN_POINT ( 'NONE',  ( -59.52287095715006160, -29.50247984919015209, -1.443849546365056913 ) ) ;
#57813=ADVANCED_FACE ( 'NONE', ( #10537 ), #21518, .T. ) ;
#57815=CARTESIAN_POINT ( 'NONE',  ( -53.54759161719780991, -24.15620529776627734, 10.23563542870660825 ) ) ;
#57816=CARTESIAN_POINT ( 'NONE',  ( -10.59417575825165159, 18.57464501519095279, 11.49999999999999645 ) ) ;
#57817=ORIENTED_EDGE ( 'NONE', *, *, #24822, .F. ) ;
#57818=PLANE ( 'NONE',  #45212 ) ;
#57819=EDGE_CURVE ( 'NONE', #58649, #67935, #84358, .T. ) ;
#57820=EDGE_LOOP ( 'NONE', ( #77404, #8535, #32538, #56910 ) ) ;
#57822=CARTESIAN_POINT ( 'NONE',  ( -2.790049085472659396, -22.09070898310802633, 11.49999999999998934 ) ) ;
#57823=CARTESIAN_POINT ( 'NONE',  ( -19.50335911044312098, -6.847048061534898977, -1.500000000000002220 ) ) ;
#57825=CARTESIAN_POINT ( 'NONE',  ( -113.5895376238167245, -24.65952944569304961, 1.056160979905703678 ) ) ;
#57826=ORIENTED_EDGE ( 'NONE', *, *, #2432, .T. ) ;
#57830=CARTESIAN_POINT ( 'NONE',  ( -3.961239394588834895, 20.55660451852329018, -1.500000000000002220 ) ) ;
#57832=CARTESIAN_POINT ( 'NONE',  ( 11.25260618158950621, 18.78031238747207610, 11.49999999999999645 ) ) ;
#57833=DIRECTION ( 'NONE',  ( -1.000000000000000000, -3.773278334444166432E-23, -8.201307841325785021E-29 ) ) ;
#57834=CARTESIAN_POINT ( 'NONE',  ( -22.50818191331092777, 0.9639279967183422837, 11.49999999999998934 ) ) ;
#57835=VECTOR ( 'NONE', #78680, 1000.000000000000114 ) ;
#57836=CARTESIAN_POINT ( 'NONE',  ( 18.03207908435136986, 10.65457695745678457, -1.500000000000002220 ) ) ;
#57837=CARTESIAN_POINT ( 'NONE',  ( -89.40841769935767047, -25.26877885127129986, 5.947789088311301597 ) ) ;
#57838=CARTESIAN_POINT ( 'NONE',  ( -106.5562042904834215, -23.47596703998600631, 11.44779298504227683 ) ) ;
#57839=CARTESIAN_POINT ( 'NONE',  ( -119.6274284003628168, -23.73791477778912551, 11.05961554403169700 ) ) ;
#57841=ADVANCED_FACE ( 'NONE', ( #70191, #31622, #93513 ), #58277, .F. ) ;
#57842=VERTEX_POINT ( 'NONE', #34143 ) ;
#57843=B_SPLINE_CURVE_WITH_KNOTS ( 'NONE', 3,
 ( #50533, #50047, #88106, #80982 ),
 .UNSPECIFIED., .F., .F.,
 ( 4, 4 ),
 ( 2.531585061196475251E-09, 0.002563035601033511121 ),
 .UNSPECIFIED. ) ;
#57844=ORIENTED_EDGE ( 'NONE', *, *, #85517, .T. ) ;
#57850=CARTESIAN_POINT ( 'NONE',  ( 10.45947017991876926, -18.73710855793504848, -1.500000000000002220 ) ) ;
#57851=ORIENTED_EDGE ( 'NONE', *, *, #34254, .F. ) ;
#57854=CARTESIAN_POINT ( 'NONE',  ( 21.06685942672242362, 1.161445541649065882, 11.49999999999998934 ) ) ;
#57857=CARTESIAN_POINT ( 'NONE',  ( -50.49351916561946751, -24.40133493613049609, 9.663955038902804162 ) ) ;
#57858=AXIS2_PLACEMENT_3D ( 'NONE', #75281, #58577, #98616 ) ;
#57859=DIRECTION ( 'NONE',  ( -3.773278334453079618E-23, 0.9999999999976377785, 2.173523156925979975E-06 ) ) ;
#57860=CARTESIAN_POINT ( 'NONE',  ( -129.6236597985572985, -24.15620529776629510, 10.23563542870659759 ) ) ;
#57861=CARTESIAN_POINT ( 'NONE',  ( 1.153593019990587942, -22.03401787307112869, -1.500000000000002220 ) ) ;
#57863=CARTESIAN_POINT ( 'NONE',  ( -65.56867036171823315, -23.48786465467241058, 11.44779295918254824 ) ) ;
#57864=DIRECTION ( 'NONE',  ( -3.773278334453079618E-23, 0.9999999999976377785, 2.173523156925979975E-06 ) ) ;
#57865=FACE_OUTER_BOUND ( 'NONE', #90055, .T. ) ;
#57868=CARTESIAN_POINT ( 'NONE',  ( -47.52287095715006160, -24.64898659630528854, 1.056161002820821038 ) ) ;
#57870=CARTESIAN_POINT ( 'NONE',  ( 21.01207135711032237, 3.775690236426352264, -1.500000000000002220 ) ) ;
#57872=CARTESIAN_POINT ( 'NONE',  ( -90.25587550125513303, -25.31768024997816724, 4.634761245912266681 ) ) ;
#57875=CARTESIAN_POINT ( 'NONE',  ( -80.94394040031853876, -25.13915873745154883, 7.007560659833019123 ) ) ;
#57876=CARTESIAN_POINT ( 'NONE',  ( 19.01167203989450982, 12.12494712425435850, -1.500000000000002220 ) ) ;
#57877=FACE_OUTER_BOUND ( 'NONE', #5640, .T. ) ;
#57878=VERTEX_POINT ( 'NONE', #63096 ) ;
#57880=CARTESIAN_POINT ( 'NONE',  ( -79.62973999110049306, -24.34968618360933945, 0.1864209137778814473 ) ) ;
#57881=CARTESIAN_POINT ( 'NONE',  ( -19.47062899137607772, 3.135797168518691169, 11.49999999999999645 ) ) ;
#57882=DIRECTION ( 'NONE',  ( 1.000000000000000000, 3.773278334444166432E-23, 8.201307841325785021E-29 ) ) ;
#57884=ADVANCED_FACE ( 'NONE', ( #94023 ), #32626, .T. ) ;
#57885=ORIENTED_EDGE ( 'NONE', *, *, #60657, .T. ) ;
#57886=PLANE ( 'NONE',  #97636 ) ;
#57887=CARTESIAN_POINT ( 'NONE',  ( -29.81175120719462157, -24.60094610731835729, 4.942812391584706866 ) ) ;
#57888=CARTESIAN_POINT ( 'NONE',  ( -113.5562042904833788, -24.64898659630528854, 1.056161002820831474 ) ) ;
#57889=CARTESIAN_POINT ( 'NONE',  ( -19.98381242416700587, 8.274006965216138099, -1.500000000000002220 ) ) ;
#57890=VECTOR ( 'NONE', #30489, 1000.000000000000114 ) ;
#57891=CARTESIAN_POINT ( 'NONE',  ( -88.52287095715006160, -23.47593901973090524, -1.443836447538996426 ) ) ;
#57893=CARTESIAN_POINT ( 'NONE',  ( -50.58953762381672448, -23.47593901973091235, -1.443836447539009749 ) ) ;
#57894=CARTESIAN_POINT ( 'NONE',  ( -81.09999867506596161, -25.06835676914625211, 7.442983283209521517 ) ) ;
#57895=CARTESIAN_POINT ( 'NONE',  ( -14.06767371131996214, 13.90018863433869889, 11.49999999999998934 ) ) ;
#57896=EDGE_LOOP ( 'NONE', ( #67478, #49432, #13231, #5742 ) ) ;
#57898=CARTESIAN_POINT ( 'NONE',  ( -20.02346298389695534, -3.155783441878276196, 11.49999999999999645 ) ) ;
#57900=ORIENTED_EDGE ( 'NONE', *, *, #94154, .F. ) ;
#57901=PLANE ( 'NONE',  #89676 ) ;
#57905=CARTESIAN_POINT ( 'NONE',  ( -120.5562042904834072, -23.48786465467241413, 11.44779295918253759 ) ) ;
#57906=CARTESIAN_POINT ( 'NONE',  ( -13.81204400269958654, 14.50282280199826701, 11.49999999999998934 ) ) ;
#57909=VECTOR ( 'NONE', #88299, 1000.000000000000114 ) ;
#57911=FACE_OUTER_BOUND ( 'NONE', #10660, .T. ) ;
#57914=CARTESIAN_POINT ( 'NONE',  ( -73.64957981708161583, -23.48783264082477018, -1.443836473390094355 ) ) ;
#57917=EDGE_CURVE ( 'NONE', #76505, #23443, #41987, .T. ) ;
#57918=CARTESIAN_POINT ( 'NONE',  ( 8.286623624103266097E-13, -23.05000000000000426, 11.49999999999999645 ) ) ;
#57919=EDGE_LOOP ( 'NONE', ( #97742, #20601, #41782, #58789 ) ) ;
#57920=ADVANCED_FACE ( 'NONE', ( #25518 ), #17909, .F. ) ;
#57921=VECTOR ( 'NONE', #61841, 1000.000000000000114 ) ;
#57922=CARTESIAN_POINT ( 'NONE',  ( 15.76184642470745700, 12.85868457875834103, 11.49999999999998934 ) ) ;
#57924=EDGE_CURVE ( 'NONE', #97996, #66785, #10513, .T. ) ;
#57925=CARTESIAN_POINT ( 'NONE',  ( -17.89994474767736676, -14.32179853049041363, -1.500000000000002220 ) ) ;
#57926=CARTESIAN_POINT ( 'NONE',  ( -32.60153195108193813, -23.96119346886880663, -0.6495511937831992544 ) ) ;
#57927=EDGE_CURVE ( 'NONE', #35458, #8654, #25006, .T. ) ;
#57931=CARTESIAN_POINT ( 'NONE',  ( -49.44941220326682441, -25.26264084044488811, 6.666982223683588060 ) ) ;
#57933=CARTESIAN_POINT ( 'NONE',  ( -21.05374637409849825, 2.266213160971460194, 11.49999999999999645 ) ) ;
#57934=CARTESIAN_POINT ( 'NONE',  ( -2.513997614918375589, -22.02279109229760223, 11.49999999999998934 ) ) ;
#57935=B_SPLINE_CURVE_WITH_KNOTS ( 'NONE', 3,
 ( #83720, #21807, #52784, #14198 ),
 .UNSPECIFIED., .F., .F.,
 ( 4, 4 ),
 ( 1.387778780781445521E-17, 9.999999999997510880E-05 ),
 .UNSPECIFIED. ) ;
#57936=CARTESIAN_POINT ( 'NONE',  ( 3.086129920417311823, 20.35385046113321295, 11.49999999999998934 ) ) ;
#57937=ORIENTED_EDGE ( 'NONE', *, *, #79560, .F. ) ;
#57938=CARTESIAN_POINT ( 'NONE',  ( -41.60818966792778184, -23.73766607897670866, -1.055555164236441801 ) ) ;
#57941=LINE ( 'NONE', #19352, #48636 ) ;
#57946=DIRECTION ( 'NONE',  ( 0.4821794293845152457, 1.904163831934039853E-06, -0.8760724843726103162 ) ) ;
#57947=CARTESIAN_POINT ( 'NONE',  ( -130.5728709571500588, -23.47596703998600631, 11.44779298504227860 ) ) ;
#57948=CARTESIAN_POINT ( 'NONE',  ( -8.830788454959730416, 18.81286502489961876, -1.500000000000002220 ) ) ;
#57949=CARTESIAN_POINT ( 'NONE',  ( -18.42844947050907578, 11.51566461966115540, 11.49999999999999645 ) ) ;
#57950=VERTEX_POINT ( 'NONE', #27526 ) ;
#57951=CARTESIAN_POINT ( 'NONE',  ( -127.6228709571500559, -24.65952944569305316, 1.056160979905707897 ) ) ;
#57953=CARTESIAN_POINT ( 'NONE',  ( -115.5535853569740965, -24.40034930558990567, 0.3402023900116066257 ) ) ;
#57954=CARTESIAN_POINT ( 'NONE',  ( 20.99545381566289137, 7.807860396396394620, -1.500000000000002220 ) ) ;
#57956=DIRECTION ( 'NONE',  ( -3.773278334453079618E-23, 0.9999999999976377785, 2.173523156925979975E-06 ) ) ;
#57958=LINE ( 'NONE', #40714, #67966 ) ;
#57960=B_SPLINE_SURFACE_WITH_KNOTS ( 'NONE', 3, 3, ( 
 ( #33387, #79060, #86179, #9553 ),
 ( #49142, #55251, #47633, #70966 ),
 ( #17166, #8561, #79567, #32397 ),
 ( #1457, #39511, #947, #1959 ),
 ( #94788, #17668, #93281, #31394 ),
 ( #63372, #25276, #69953, #56255 ),
 ( #48641, #94286, #41018, #31897 ),
 ( #24770, #10055, #62872, #64376 ),
 ( #441, #95296, #8054, #56756 ),
 ( #87685, #39003, #93788, #55752 ) ),
 .UNSPECIFIED., .F., .F., .F.,
 ( 4, 3, 3, 4 ),
 ( 4, 4 ),
 ( 0.7022005934521633463, 0.7765311282011415628, 0.8508616629501198902, 0.9995227324480764342 ),
 ( 0.6995784262351472105, 0.7010080898895992840 ),
 .UNSPECIFIED. ) ;
#57964=CARTESIAN_POINT ( 'NONE',  ( -87.62287095715005592, -23.72747288104441665, -1.053458166803660889 ) ) ;
#57966=CARTESIAN_POINT ( 'NONE',  ( 19.98919582620916913, -7.218065965386815996, -1.500000000000002220 ) ) ;
#57967=ORIENTED_EDGE ( 'NONE', *, *, #3128, .T. ) ;
#57969=CARTESIAN_POINT ( 'NONE',  ( -0.06377455873143267340, 21.83884041771831619, 11.49999999999998934 ) ) ;
#57970=CARTESIAN_POINT ( 'NONE',  ( -52.55339013111201751, -23.96169478059712787, 10.65365249895718769 ) ) ;
#57971=CARTESIAN_POINT ( 'NONE',  ( 8.023449251107201974, -21.19570997880782670, 11.49999999999998934 ) ) ;
#57972=CARTESIAN_POINT ( 'NONE',  ( -41.39385049892748469, -25.18430990895221200, 3.844044810517027955 ) ) ;
#57973=CARTESIAN_POINT ( 'NONE',  ( -49.52287095715008292, -23.96177878511307213, 10.65340807706330217 ) ) ;
#57974=CARTESIAN_POINT ( 'NONE',  ( 21.07893183998518438, -5.767110019903106455, -1.500000000000002220 ) ) ;
#57975=CARTESIAN_POINT ( 'NONE',  ( -66.62287095715004170, -24.51283580621365132, 0.6167428607019709297 ) ) ;
#57978=CARTESIAN_POINT ( 'NONE',  ( -49.18705952543585624, -25.12782698363243128, 7.035471548030500344 ) ) ;
#57980=VECTOR ( 'NONE', #51244, 1000.000000000000114 ) ;
#57982=CARTESIAN_POINT ( 'NONE',  ( -30.62558287684645109, -24.04478067413149844, -0.4748248766032758805 ) ) ;
#57984=CARTESIAN_POINT ( 'NONE',  ( -113.5228709571500616, -23.47593901973090524, -1.443836447538996204 ) ) ;
#57985=CARTESIAN_POINT ( 'NONE',  ( -0.05083659990941549051, -22.39188026470795023, 1.363349870542264863 ) ) ;
#57986=CARTESIAN_POINT ( 'NONE',  ( -12.29646723538143505, -17.35194501319736560, -1.500000000000002220 ) ) ;
#57988=CARTESIAN_POINT ( 'NONE',  ( -26.30595710371889950, -24.97064650647640249, 3.418818890720438208 ) ) ;
#57990=DIRECTION ( 'NONE',  ( -0.9796516281416185468, 4.362379964674604143E-07, -0.2007054744626703968 ) ) ;
#57992=CARTESIAN_POINT ( 'NONE',  ( -84.62287095715007013, -23.48786465467241769, 11.44779295918254469 ) ) ;
#57995=ORIENTED_EDGE ( 'NONE', *, *, #22735, .T. ) ;
#57996=CARTESIAN_POINT ( 'NONE',  ( 12.07855387261060898, -15.37489856218140183, 11.49999999999999645 ) ) ;
#57998=VECTOR ( 'NONE', #78659, 1000.000000000000114 ) ;
#58000=B_SPLINE_CURVE_WITH_KNOTS ( 'NONE', 3,
 ( #59952, #21353, #44220, #99970, #69553, #98479, #91374, #32, #52328, #20860, #28979, #51833, #30479, #75641 ),
 .UNSPECIFIED., .F., .F.,
 ( 4, 2, 2, 2, 2, 2, 4 ),
 ( 8.673617379884035472E-19, 0.0002414200208935323767, 0.0004828400417870638861, 0.0009656800835741269047, 0.001448520125361189978, 0.001689940146254730784, 0.001931360167148271807 ),
 .UNSPECIFIED. ) ;
#58001=CARTESIAN_POINT ( 'NONE',  ( -79.34892427156343331, -25.26180990464883180, 6.036045387136124596 ) ) ;
#58002=ORIENTED_EDGE ( 'NONE', *, *, #9781, .F. ) ;
#58003=FACE_OUTER_BOUND ( 'NONE', #60581, .T. ) ;
#58004=CARTESIAN_POINT ( 'NONE',  ( -99.63322708413970474, -25.31439593098938801, 5.473920184482165219 ) ) ;
#58005=CARTESIAN_POINT ( 'NONE',  ( -90.52287095715003318, -23.85196035786899671, -0.8779234886475166810 ) ) ;
#58006=CARTESIAN_POINT ( 'NONE',  ( -60.52287095715008292, -23.85196035786900737, -0.8779234886475210109 ) ) ;
#58007=CARTESIAN_POINT ( 'NONE',  ( 9.442166470422634461, 17.27452087139410963, -1.500000000000002220 ) ) ;
#58008=ORIENTED_EDGE ( 'NONE', *, *, #12535, .F. ) ;
#58009=CARTESIAN_POINT ( 'NONE',  ( -94.62287095715005592, -24.64898659630528854, 1.056161002820827921 ) ) ;
#58012=ORIENTED_EDGE ( 'NONE', *, *, #31847, .F. ) ;
#58015=PLANE ( 'NONE',  #31285 ) ;
#58016=CARTESIAN_POINT ( 'NONE',  ( -76.52287095715007581, -23.47593901973090169, -1.443836447538996648 ) ) ;
#58019=CARTESIAN_POINT ( 'NONE',  ( -114.5206646555255503, -23.73791477778912196, 11.05961554403169700 ) ) ;
#58020=CARTESIAN_POINT ( 'NONE',  ( 12.75013301566243129, -15.34773647900153115, 11.49999999999998934 ) ) ;
#58021=CARTESIAN_POINT ( 'NONE',  ( -0.03132738354372287259, -22.64444240169225253, 8.124201566845400180 ) ) ;
#58022=CARTESIAN_POINT ( 'NONE',  ( -0.2410636032128395945, 19.88167143085883737, -1.500000000000002220 ) ) ;
#58025=DIRECTION ( 'NONE',  ( -3.773278334453079618E-23, 0.9999999999976377785, 2.173523156925979975E-06 ) ) ;
#58027=CARTESIAN_POINT ( 'NONE',  ( -70.52287095715007581, -23.48783264082477018, -1.443836473390089914 ) ) ;
#58029=CARTESIAN_POINT ( 'NONE',  ( 5.171613189315443115, 20.13430294385436881, 11.49999999999999645 ) ) ;
#58031=B_SPLINE_CURVE_WITH_KNOTS ( 'NONE', 3,
 ( #90667, #91162, #13529, #75426 ),
 .UNSPECIFIED., .F., .F.,
 ( 4, 4 ),
 ( 0.8611149010728148534, 0.8701213323449306092 ),
 .UNSPECIFIED. ) ;
#58033=CARTESIAN_POINT ( 'NONE',  ( -7.756741253720922380, -21.46081514045699024, 11.49999999999999645 ) ) ;
#58034=EDGE_LOOP ( 'NONE', ( #35003, #93219, #61571, #16075 ) ) ;
#58037=DIRECTION ( 'NONE',  ( 0.000000000000000000, -2.173523156925980399E-06, 0.9999999999976378895 ) ) ;
#58039=ADVANCED_FACE ( 'NONE', ( #73205 ), #6141, .T. ) ;
#58040=CARTESIAN_POINT ( 'NONE',  ( 3.706880958665978998, 19.89330832657401515, 11.49999999999998934 ) ) ;
#58042=PLANE ( 'NONE',  #43684 ) ;
#58043=ADVANCED_FACE ( 'NONE', ( #52355 ), #73339, .T. ) ;
#58045=EDGE_CURVE ( 'NONE', #77563, #34509, #61970, .T. ) ;
#58047=CARTESIAN_POINT ( 'NONE',  ( -79.34850868052345163, -25.28330624484387101, 5.890934297546558618 ) ) ;
#58049=CARTESIAN_POINT ( 'NONE',  ( -16.07871291144651593, -12.00523380332558965, -1.500000000000002220 ) ) ;
#58051=CARTESIAN_POINT ( 'NONE',  ( 19.40125262130244366, -8.172613994405130811, 11.49999999999999645 ) ) ;
#58052=CARTESIAN_POINT ( 'NONE',  ( -50.40895856474225667, -29.50249942614373921, 7.563164501610022405 ) ) ;
#58054=CARTESIAN_POINT ( 'NONE',  ( 18.22792733936863030, -12.41963300964812156, 11.49999999999998934 ) ) ;
#58057=CARTESIAN_POINT ( 'NONE',  ( -39.59566294291796140, -25.31589243397437627, 4.684364548415942409 ) ) ;
#58058=LINE ( 'NONE', #10359, #46790 ) ;
#58060=DIRECTION ( 'NONE',  ( 0.000000000000000000, 0.9999999999976377785, 2.173523156925979128E-06 ) ) ;
#58062=ORIENTED_EDGE ( 'NONE', *, *, #72494, .T. ) ;
#58063=VECTOR ( 'NONE', #66031, 1000.000000000000114 ) ;
#58065=CARTESIAN_POINT ( 'NONE',  ( -41.62287095715006302, -23.48786465467240703, 11.44779295918255180 ) ) ;
#58066=CARTESIAN_POINT ( 'NONE',  ( -30.47287095715007510, -29.50248298729120222, -6.412432995908637812E-05 ) ) ;
#58067=CARTESIAN_POINT ( 'NONE',  ( -58.62287095715006302, -24.51283580621364067, 0.6167428607019806996 ) ) ;
#58069=CARTESIAN_POINT ( 'NONE',  ( 15.34425395324244867, 13.73259486114767114, -1.500000000000002220 ) ) ;
#58070=CARTESIAN_POINT ( 'NONE',  ( 0.7969447072908428797, -21.54811710690876225, 11.49999999999999645 ) ) ;
#58075=CARTESIAN_POINT ( 'NONE',  ( 8.793911523065595759, -20.50603677605392150, 11.49999999999998934 ) ) ;
#58080=CARTESIAN_POINT ( 'NONE',  ( -51.04357394935764347, -25.30543060587211812, 4.940877950953177056 ) ) ;
#58081=VECTOR ( 'NONE', #85958, 1000.000000000000114 ) ;
#58082=CARTESIAN_POINT ( 'NONE',  ( 18.76864855846692492, -9.085702381504452418, -1.500000000000002220 ) ) ;
#58083=ORIENTED_EDGE ( 'NONE', *, *, #40823, .T. ) ;
#58085=ORIENTED_EDGE ( 'NONE', *, *, #31445, .T. ) ;
#58086=EDGE_LOOP ( 'NONE', ( #3625, #10651, #4736, #19302 ) ) ;
#58087=CARTESIAN_POINT ( 'NONE',  ( -50.44234050327818153, -25.30264421209000858, 4.735024738193449600 ) ) ;
#58088=CARTESIAN_POINT ( 'NONE',  ( 4.297136154115697160, 20.59472113332480703, -1.500000000000002220 ) ) ;
#58089=ORIENTED_EDGE ( 'NONE', *, *, #12527, .T. ) ;
#58092=CARTESIAN_POINT ( 'NONE',  ( -120.6253516754611610, -24.52399227489125266, 9.353111116836528183 ) ) ;
#58093=CARTESIAN_POINT ( 'NONE',  ( -76.55010092559956547, -24.15620529776628089, 10.23563542870660470 ) ) ;
#58095=CARTESIAN_POINT ( 'NONE',  ( -10.76533847658563126, -18.86179312034942868, -1.500000000000002220 ) ) ;
#58096=CARTESIAN_POINT ( 'NONE',  ( -97.62287095715005592, -24.64965695001468404, 8.947790433994178727 ) ) ;
#58097=CARTESIAN_POINT ( 'NONE',  ( 18.30470771955606679, 12.64531542519679697, 11.49999999999999645 ) ) ;
#58101=EDGE_CURVE ( 'NONE', #81001, #32994, #51672, .T. ) ;
#58102=CARTESIAN_POINT ( 'NONE',  ( -106.5228709571500758, -24.64965694238408034, 8.947790433994192938 ) ) ;
#58103=ORIENTED_EDGE ( 'NONE', *, *, #18529, .T. ) ;
#58104=CARTESIAN_POINT ( 'NONE',  ( -36.52287095715006870, -23.47596703998600631, 11.44779298504229281 ) ) ;
#58105=ORIENTED_EDGE ( 'NONE', *, *, #66769, .F. ) ;
#58107=VERTEX_POINT ( 'NONE', #14267 ) ;
#58109=EDGE_CURVE ( 'NONE', #10587, #3669, #73425, .T. ) ;
#58110=DIRECTION ( 'NONE',  ( -3.773278334453079618E-23, 0.9999999999976377785, 2.173523156925979975E-06 ) ) ;
#58113=CARTESIAN_POINT ( 'NONE',  ( -126.5228709571500048, -23.95044443724992789, 10.65354141964648882 ) ) ;
#58115=CARTESIAN_POINT ( 'NONE',  ( -130.5728709571500303, -24.76085724621141182, 8.931194175204877794 ) ) ;
#58116=CARTESIAN_POINT ( 'NONE',  ( 6.846561153812083411, -21.39451737393737574, -1.500000000000002220 ) ) ;
#58118=CARTESIAN_POINT ( 'NONE',  ( -86.52287095715006160, -29.50250243563736774, 8.947779886222139822 ) ) ;
#58121=LINE ( 'NONE', #17537, #77329 ) ;
#58122=CARTESIAN_POINT ( 'NONE',  ( -130.5728709571500588, -25.14081846633249384, 7.291654623549831626 ) ) ;
#58123=CARTESIAN_POINT ( 'NONE',  ( 0.9049686737998731134, -19.58615294826029540, 11.49999999999998934 ) ) ;
#58124=CARTESIAN_POINT ( 'NONE',  ( -50.17515359291254384, -25.31218963190688953, 4.714858780549761264 ) ) ;
#58125=ORIENTED_EDGE ( 'NONE', *, *, #48241, .T. ) ;
#58126=CARTESIAN_POINT ( 'NONE',  ( -18.46100929034391314, -11.06139713797464985, -1.500000000000002220 ) ) ;
#58128=CARTESIAN_POINT ( 'NONE',  ( -71.30376622360817862, -25.25639414126157689, 6.239614501453647932 ) ) ;
#58129=CARTESIAN_POINT ( 'NONE',  ( -101.6833297298926055, -25.24379662554390436, 3.680570895106967999 ) ) ;
#58131=CARTESIAN_POINT ( 'NONE',  ( -22.63010559926462051, 4.001702944626347680, -1.500000000000002220 ) ) ;
#58135=CARTESIAN_POINT ( 'NONE',  ( -49.54717124518386129, -24.15543982623906771, -0.2315651400026657036 ) ) ;
#58136=CARTESIAN_POINT ( 'NONE',  ( 20.09017895974002599, 0.4902201509063087159, 11.49999999999999645 ) ) ;
#58138=CARTESIAN_POINT ( 'NONE',  ( -32.57491724666229516, -24.66019654487198665, 8.947790411086131712 ) ) ;
#58140=CARTESIAN_POINT ( 'NONE',  ( -79.52287095715006160, -24.64898659630367916, 1.056161002820826145 ) ) ;
#58142=CARTESIAN_POINT ( 'NONE',  ( -5.703961651189128901, -19.02375728206049743, 11.49999999999998934 ) ) ;
#58143=CARTESIAN_POINT ( 'NONE',  ( -113.5585636484403267, -23.48783264082477373, -1.443836473390084807 ) ) ;
#58144=CARTESIAN_POINT ( 'NONE',  ( 13.13437215454093199, 14.66711140016434278, -1.500000000000002220 ) ) ;
#58149=CARTESIAN_POINT ( 'NONE',  ( 1.647368763193059582, 20.57021071130147405, 11.49999999999999645 ) ) ;
#58150=CARTESIAN_POINT ( 'NONE',  ( -42.62287095715003460, -24.51283580621364422, 0.6167428607019693754 ) ) ;
#58151=CARTESIAN_POINT ( 'NONE',  ( -2.225104987405961854, -22.55768739424384606, 11.49999999999999645 ) ) ;
#58152=ORIENTED_EDGE ( 'NONE', *, *, #8238, .F. ) ;
#58153=FACE_OUTER_BOUND ( 'NONE', #8884, .T. ) ;
#58154=CARTESIAN_POINT ( 'NONE',  ( -56.52287095715006870, -24.65952944569304606, 1.056160979905695463 ) ) ;
#58156=CARTESIAN_POINT ( 'NONE',  ( -27.40807623642065494, -24.93063630324751045, 8.230615498763011573 ) ) ;
#58161=CARTESIAN_POINT ( 'NONE',  ( -18.82434810282327220, -12.99595988342530362, -1.500000000000002220 ) ) ;
#58163=CARTESIAN_POINT ( 'NONE',  ( 20.07693369621832602, 7.961103810760662647, -1.500000000000002220 ) ) ;
#58164=CARTESIAN_POINT ( 'NONE',  ( -37.52287095715006870, -24.64965694238406613, 8.947790433994205372 ) ) ;
#58166=EDGE_CURVE ( 'NONE', #19170, #97996, #64497, .T. ) ;
#58167=CARTESIAN_POINT ( 'NONE',  ( -0.2110286175373513040, -22.56517410205234597, 11.49999999999999645 ) ) ;
#58168=ORIENTED_EDGE ( 'NONE', *, *, #50345, .F. ) ;
#58169=CARTESIAN_POINT ( 'NONE',  ( -89.81226385320384509, -25.06732983082694943, 7.447789526168956620 ) ) ;
#58170=CARTESIAN_POINT ( 'NONE',  ( 19.17116566557315949, -10.70166234769870961, -1.500000000000002220 ) ) ;
#58171=EDGE_CURVE ( 'NONE', #71061, #12190, #3080, .T. ) ;
#58174=EDGE_LOOP ( 'NONE', ( #60091, #38367, #17241, #81357 ) ) ;
#58175=CARTESIAN_POINT ( 'NONE',  ( -89.62287095715007013, -24.35013146730204525, 9.818937971375106599 ) ) ;
#58176=CARTESIAN_POINT ( 'NONE',  ( -47.52287095715006160, -23.47596703998600631, 11.44779298504229104 ) ) ;
#58177=ORIENTED_EDGE ( 'NONE', *, *, #48419, .F. ) ;
#58178=DIRECTION ( 'NONE',  ( -3.773278334453079030E-23, 0.9999999999976377785, 2.173523156925979128E-06 ) ) ;
#58181=ORIENTED_EDGE ( 'NONE', *, *, #22674, .F. ) ;
#58182=ORIENTED_EDGE ( 'NONE', *, *, #65379, .F. ) ;
#58184=CARTESIAN_POINT ( 'NONE',  ( -70.62287095715005592, -29.50247984919015209, -1.443849546365055359 ) ) ;
#58186=EDGE_CURVE ( 'NONE', #80701, #25971, #7983, .T. ) ;
#58187=CARTESIAN_POINT ( 'NONE',  ( -10.90597124047809530, 17.21661415904998904, -1.500000000000002220 ) ) ;
#58188=VERTEX_POINT ( 'NONE', #39619 ) ;
#58190=AXIS2_PLACEMENT_3D ( 'NONE', #36455, #28342, #68412 ) ;
#58191=CARTESIAN_POINT ( 'NONE',  ( -92.52287095715010423, -23.73934037231756733, 11.05740245334328620 ) ) ;
#58192=CARTESIAN_POINT ( 'NONE',  ( -105.5074323697901377, -25.00158670708910691, 2.256160236439218369 ) ) ;
#58193=CARTESIAN_POINT ( 'NONE',  ( -57.52287095715003318, -23.48783264082476663, -1.443836473390093911 ) ) ;
#58195=FACE_OUTER_BOUND ( 'NONE', #52907, .T. ) ;
#58196=CARTESIAN_POINT ( 'NONE',  ( -89.92287095715005307, -23.47593901973090524, -1.443836447538996870 ) ) ;
#58197=VERTEX_POINT ( 'NONE', #40635 ) ;
#58198=VECTOR ( 'NONE', #80475, 1000.000000000000114 ) ;
#58199=CARTESIAN_POINT ( 'NONE',  ( -13.51810693421681719, -15.76408947421354156, 11.49999999999998934 ) ) ;
#58201=CARTESIAN_POINT ( 'NONE',  ( -31.52287095715006160, -23.48786465467240347, 11.44779295918255357 ) ) ;
#58203=DIRECTION ( 'NONE',  ( -3.773278334453080206E-23, 0.9999999999976377785, 2.173523156925979975E-06 ) ) ;
#58207=CARTESIAN_POINT ( 'NONE',  ( -88.52287095715006160, -24.65952944569304606, 1.056160979905700570 ) ) ;
#58210=CARTESIAN_POINT ( 'NONE',  ( -52.62287095715005592, -23.73934037231757088, 11.05740245334329153 ) ) ;
#58211=CARTESIAN_POINT ( 'NONE',  ( -70.97512524164069703, -25.31201633795301831, 5.512439363672202219 ) ) ;
#58212=EDGE_CURVE ( 'NONE', #46960, #15342, #44300, .T. ) ;
#58213=CARTESIAN_POINT ( 'NONE',  ( 20.57361055066190758, -8.084994430987380909, 11.49999999999999645 ) ) ;
#58214=ORIENTED_EDGE ( 'NONE', *, *, #10309, .T. ) ;
#58215=CARTESIAN_POINT ( 'NONE',  ( -108.6313998591546550, -23.73766607897671932, -1.055555164236429366 ) ) ;
#58216=CARTESIAN_POINT ( 'NONE',  ( 22.48748499206561746, 2.281147167042596013, 11.49999999999998934 ) ) ;
#58217=CARTESIAN_POINT ( 'NONE',  ( -46.52287095715006870, -24.51387760970725083, 9.387446482453420060 ) ) ;
#58219=EDGE_CURVE ( 'NONE', #58835, #56230, #46811, .T. ) ;
#58220=VERTEX_POINT ( 'NONE', #1576 ) ;
#58223=ADVANCED_FACE ( 'NONE', ( #94407 ), #41139, .F. ) ;
#58225=EDGE_CURVE ( 'NONE', #44828, #13092, #72092, .T. ) ;
#58226=B_SPLINE_SURFACE_WITH_KNOTS ( 'NONE', 3, 1, ( 
 ( #3615, #11704 ),
 ( #26942, #50290 ),
 ( #66034, #42685 ),
 ( #21805, #92326 ),
 ( #36048, #67023 ),
 ( #7096, #45174 ),
 ( #68501, #13194 ),
 ( #14702, #37048 ),
 ( #28427, #61403 ),
 ( #59391, #6095 ),
 ( #52782, #68008 ),
 ( #84211, #44169 ),
 ( #59904, #91329 ),
 ( #12701, #30433 ),
 ( #13698, #90334 ) ),
 .UNSPECIFIED., .F., .F., .F.,
 ( 4, 1, 1, 1, 1, 1, 1, 1, 1, 1, 1, 1, 4 ),
 ( 2, 2 ),
 ( 0.000000000000000000, 0.08968993624739593495, 0.1784940104960813789, 0.2668377532994903878, 0.3565581760610176398, 0.4453342496549802521, 0.5308058350374902368, 0.6140762174402841778, 0.6977070858228016093, 0.7791419498114620090, 0.8553535905869761313, 0.9285568200856556542, 1.000000000000000000 ),
 ( 0.000000000000000000, 1.000000000000000000 ),
 .UNSPECIFIED. ) ;
#58227=CARTESIAN_POINT ( 'NONE',  ( -86.52287095715006160, -23.48783264083431277, -1.443836473375255336 ) ) ;
#58229=CARTESIAN_POINT ( 'NONE',  ( -19.86647519178106691, -7.318714840676754818, 11.49999999999998934 ) ) ;
#58231=CARTESIAN_POINT ( 'NONE',  ( -41.80321513992567617, -25.30077457980579680, 4.650809782510233248 ) ) ;
#58232=CARTESIAN_POINT ( 'NONE',  ( -16.22183044023116238, -15.26045173261249310, -1.500000000000002220 ) ) ;
#58235=LINE ( 'NONE', #20642, #46517 ) ;
#58236=CARTESIAN_POINT ( 'NONE',  ( -44.62287095715004881, -24.64898659630528854, 1.056161002820819261 ) ) ;
#58237=CARTESIAN_POINT ( 'NONE',  ( -36.52201391965095212, -23.48786465467240347, 11.44779295918255180 ) ) ;
#58239=CARTESIAN_POINT ( 'NONE',  ( -3.338044803349280443, -19.22079736023769669, 11.49999999999998934 ) ) ;
#58240=CARTESIAN_POINT ( 'NONE',  ( -4.378498130703003532, 20.98420022172975763, -1.500000000000002220 ) ) ;
#58242=LINE ( 'NONE', #74451, #1694 ) ;
#58243=CARTESIAN_POINT ( 'NONE',  ( -77.53983134128570498, -24.65952944569304606, 1.056160979905701458 ) ) ;
#58244=CARTESIAN_POINT ( 'NONE',  ( 21.74077840044056842, -6.890983112422549794, -1.500000000000002220 ) ) ;
#58246=CARTESIAN_POINT ( 'NONE',  ( -102.6235476894606791, -24.65952944569305316, 1.056160979905705677 ) ) ;
#58248=CARTESIAN_POINT ( 'NONE',  ( 19.20567810191101898, 5.375360269454119155, 11.49999999999999645 ) ) ;
#58249=CARTESIAN_POINT ( 'NONE',  ( -111.6228709571500417, -24.66019654487199730, 8.947790411086124607 ) ) ;
#58250=EDGE_CURVE ( 'NONE', #27723, #24726, #18947, .T. ) ;
#58251=AXIS2_PLACEMENT_3D ( 'NONE', #85972, #63661, #94583 ) ;
#58253=CARTESIAN_POINT ( 'NONE',  ( -48.58199726423757170, -24.51314013834315375, 0.6176544820404137326 ) ) ;
#58257=CARTESIAN_POINT ( 'NONE',  ( 17.51545567653809954, -12.82042131148251229, 11.49999999999998934 ) ) ;
#58258=EDGE_CURVE ( 'NONE', #1776, #94542, #17696, .T. ) ;
#58259=CARTESIAN_POINT ( 'NONE',  ( -67.62287095715005592, -24.65952944569304606, 1.056160979905697017 ) ) ;
#58261=CARTESIAN_POINT ( 'NONE',  ( 7.694069055508638399, 17.95645395709951941, -1.500000000000002220 ) ) ;
#58262=B_SPLINE_CURVE_WITH_KNOTS ( 'NONE', 3,
 ( #17883, #25492, #63577, #63069 ),
 .UNSPECIFIED., .F., .F.,
 ( 4, 4 ),
 ( 0.000000000000000000, 9.999999999999592548E-05 ),
 .UNSPECIFIED. ) ;
#58263=EDGE_CURVE ( 'NONE', #66289, #54444, #75054, .T. ) ;
#58264=CARTESIAN_POINT ( 'NONE',  ( -93.52287095715006160, -24.65952944569304606, 1.056160979905700570 ) ) ;
#58265=AXIS2_PLACEMENT_3D ( 'NONE', #47796, #23423, #64048 ) ;
#58267=AXIS2_PLACEMENT_3D ( 'NONE', #21925, #52905, #14318 ) ;
#58268=CARTESIAN_POINT ( 'NONE',  ( -69.62287095715004170, -24.50321055353805733, 9.387540953477536476 ) ) ;
#58269=CARTESIAN_POINT ( 'NONE',  ( 5.749347661499963458, 19.61174949527739386, 11.49999999999999645 ) ) ;
#58270=CARTESIAN_POINT ( 'NONE',  ( -49.53202264565179291, -25.29391963383437769, 5.541708595187663455 ) ) ;
#58273=VERTEX_POINT ( 'NONE', #57379 ) ;
#58277=( BOUNDED_SURFACE ( )  B_SPLINE_SURFACE ( 3, 1, ( 
 ( #85916, #7282 ),
 ( #21998, #38233 ),
 ( #69188, #18406 ),
 ( #16901, #9791 ),
 ( #40246, #39735 ),
 ( #70691, #49374 ),
 ( #79294, #95029 ),
 ( #56985, #2197 ),
 ( #95530, #26015 ),
 ( #1185, #80305 ),
 ( #55988, #3201 ),
 ( #10797, #78785 ),
 ( #65110, #48869 ),
 ( #56492, #9281 ),
 ( #64616, #63602 ),
 ( #71198, #32123 ),
 ( #87923, #33636 ),
 ( #87413, #78288 ),
 ( #41761, #96030 ),
 ( #72706, #79797 ) ),
 .UNSPECIFIED., .F., .F., .T. ) 
 B_SPLINE_SURFACE_WITH_KNOTS ( ( 4, 3, 1, 1, 3, 3, 1, 1, 3, 4 ),
 ( 2, 2 ),
 ( 0.000000000000000000, 0.1255889732084985166, 0.1669421422606964800, 0.2082953113128944156, 0.2496484803650923789, 0.7477322152634136021, 0.7890853843156119263, 0.8304385533678104725, 0.8717917224200087967, 1.000000000000000000 ),
 ( 0.000000000000000000, 1.000000000000000000 ),
 .UNSPECIFIED. ) 
 GEOMETRIC_REPRESENTATION_ITEM ( )  RATIONAL_B_SPLINE_SURFACE ( (
 ( 0.9999602609241470264, 0.9999602609241470264),
 ( 0.9987387818499366965, 0.9987387818499366965),
 ( 0.9998573533027315108, 0.9998573533027315108),
 ( 1.003315975282531802, 1.003315975282531802),
 ( 1.003315975282531802, 1.003315975282531802),
 ( 1.003315975282531802, 1.003315975282531802),
 ( 1.003315975282531802, 1.003315975282531802),
 ( 1.003315975282531802, 1.003315975282531802),
 ( 1.003315975282531802, 1.003315975282531802),
 ( 0.9773170091682806815, 0.9773170091682806815),
 ( 0.9773170091682806815, 0.9773170091682806815),
 ( 1.003315975282531802, 1.003315975282531802),
 ( 1.003315975282531802, 1.003315975282531802),
 ( 1.003315975282531802, 1.003315975282531802),
 ( 1.003315975282531802, 1.003315975282531802),
 ( 1.003315975282531802, 1.003315975282531802),
 ( 1.003315975282531802, 1.003315975282531802),
 ( 0.9997852197113853423, 0.9997852197113853423),
 ( 0.9986931415022445302, 0.9986931415022445302),
 ( 1.000039740655109810, 1.000039740655109810) ) ) 
 REPRESENTATION_ITEM ( '' )  SURFACE ( )  );
#58278=EDGE_CURVE ( 'NONE', #80473, #38812, #61387, .T. ) ;
#58279=CARTESIAN_POINT ( 'NONE',  ( -109.5507803029036182, -24.51314013834315375, 0.6176544820404177294 ) ) ;
#58282=CARTESIAN_POINT ( 'NONE',  ( -7.281717392095591102, 21.80608952751712692, 11.49999999999999645 ) ) ;
#58283=CARTESIAN_POINT ( 'NONE',  ( -6.081610112697643622, 21.96313418072945822, -1.500000000000002220 ) ) ;
#58285=LINE ( 'NONE', #27324, #83596 ) ;
#58288=CARTESIAN_POINT ( 'NONE',  ( -69.84651095272120358, -25.15148347341441948, 6.994331270845397519 ) ) ;
#58289=CARTESIAN_POINT ( 'NONE',  ( -21.08706934527708654, 5.832127334627817739, -1.500000000000002220 ) ) ;
#58291=CARTESIAN_POINT ( 'NONE',  ( -61.24303308397303880, -29.50249942614373921, 7.563164501610022405 ) ) ;
#58292=ADVANCED_FACE ( 'NONE', ( #82179, #20268, #35018 ), #68547, .T. ) ;
#58293=CARTESIAN_POINT ( 'NONE',  ( -28.62287095715005947, -24.34879252677621153, 0.6165374033617160299 ) ) ;
#58294=CARTESIAN_POINT ( 'NONE',  ( -64.52287095715006160, -23.48783264082476308, -1.443836473390094355 ) ) ;
#58295=DIRECTION ( 'NONE',  ( -3.773278334453079618E-23, 0.9999999999976377785, 2.173523156925978705E-06 ) ) ;
#58297=CARTESIAN_POINT ( 'NONE',  ( -3.558151220431595707, 20.12126150705307381, -1.500000000000002220 ) ) ;
#58298=ORIENTED_EDGE ( 'NONE', *, *, #77713, .T. ) ;
#58299=VERTEX_POINT ( 'NONE', #11178 ) ;
#58302=CARTESIAN_POINT ( 'NONE',  ( -21.58539018223340022, -8.019882488244659768, 11.49999999999998934 ) ) ;
#58304=EDGE_CURVE ( 'NONE', #32034, #74478, #66494, .T. ) ;
#58305=CARTESIAN_POINT ( 'NONE',  ( 7.141438900065890216, -18.84860497471923679, -1.500000000000002220 ) ) ;
#58306=VERTEX_POINT ( 'NONE', #26900 ) ;
#58308=FACE_OUTER_BOUND ( 'NONE', #66533, .T. ) ;
#58310=DIRECTION ( 'NONE',  ( -3.773278334453079030E-23, 0.9999999999976377785, 2.173523156925979128E-06 ) ) ;
#58311=PLANE ( 'NONE',  #2648 ) ;
#58312=CARTESIAN_POINT ( 'NONE',  ( -17.73838780825237649, 11.93509662624355450, 11.49999999999999645 ) ) ;
#58314=LINE ( 'NONE', #71146, #12811 ) ;
#58316=CARTESIAN_POINT ( 'NONE',  ( 20.70802603420765564, 8.137917507125113303, 11.49999999999998934 ) ) ;
#58317=CARTESIAN_POINT ( 'NONE',  ( -16.33875328525262560, 12.67428768300982256, 11.49999999999998934 ) ) ;
#58319=ORIENTED_EDGE ( 'NONE', *, *, #99229, .T. ) ;
#58321=ORIENTED_EDGE ( 'NONE', *, *, #23539, .T. ) ;
#58326=CARTESIAN_POINT ( 'NONE',  ( -9.975069251262826953, -18.38325097723136992, -1.500000000000002220 ) ) ;
#58327=CARTESIAN_POINT ( 'NONE',  ( 15.24057855588860377, 15.72025634131890470, 11.49999999999999645 ) ) ;
#58328=CARTESIAN_POINT ( 'NONE',  ( -26.71877946146332050, -24.77993706282625297, 7.184564732929184849 ) ) ;
#58329=CARTESIAN_POINT ( 'NONE',  ( 3.368619518803146029, -22.26131067175759881, 11.49999999999998934 ) ) ;
#58331=CARTESIAN_POINT ( 'NONE',  ( -2.499008156623981236, -20.81284420272260860, -1.500000000000002220 ) ) ;
#58332=CARTESIAN_POINT ( 'NONE',  ( -110.5228709571500900, -24.62226745350443480, 0.9660975649729556247 ) ) ;
#58334=CARTESIAN_POINT ( 'NONE',  ( -119.5920073095941945, -23.73791477778912551, 11.05961554403169700 ) ) ;
#58336=ADVANCED_FACE ( 'NONE', ( #50744 ), #37759, .T. ) ;
#58338=AXIS2_PLACEMENT_3D ( 'NONE', #47436, #95603, #56562 ) ;
#58339=ORIENTED_EDGE ( 'NONE', *, *, #55074, .T. ) ;
#58342=CARTESIAN_POINT ( 'NONE',  ( -44.52287095715007581, -24.35013146730204525, 9.818937971375103047 ) ) ;
#58344=AXIS2_PLACEMENT_3D ( 'NONE', #9792, #63097, #48870 ) ;
#58345=CARTESIAN_POINT ( 'NONE',  ( 0.6623178260406717976, 21.47796536025111536, -1.500000000000002220 ) ) ;
#58348=CARTESIAN_POINT ( 'NONE',  ( -19.97109070424261645, 6.737033823242594366, 11.49999999999998934 ) ) ;
#58350=CARTESIAN_POINT ( 'NONE',  ( -52.62287095715006302, -24.65952944569304250, 1.056160979905695685 ) ) ;
#58352=CARTESIAN_POINT ( 'NONE',  ( -101.5932192411211616, -23.96119346886880663, -0.6495511937832048055 ) ) ;
#58354=CARTESIAN_POINT ( 'NONE',  ( -19.11006845027251799, 11.06304553819242642, -1.500000000000002220 ) ) ;
#58356=CARTESIAN_POINT ( 'NONE',  ( -81.63319337029726341, -24.15620529776628445, 10.23563542870661180 ) ) ;
#58357=CARTESIAN_POINT ( 'NONE',  ( -65.52287095715006160, -29.50250786944525672, 11.44777988621623699 ) ) ;
#58358=CARTESIAN_POINT ( 'NONE',  ( -78.62287095715011276, -24.35013146730204525, 9.818937971375108376 ) ) ;
#58359=CARTESIAN_POINT ( 'NONE',  ( -62.60383890414039598, -23.73791477778912196, 11.05961554403171121 ) ) ;
#58360=B_SPLINE_CURVE_WITH_KNOTS ( 'NONE', 3,
 ( #45011, #29770, #35528, #91659, #80693, #52610 ),
 .UNSPECIFIED., .F., .F.,
 ( 4, 2, 4 ),
 ( 6.384118696603436915E-06, 0.001386860460837369309, 0.002767336802978134953 ),
 .UNSPECIFIED. ) ;
#58361=DIRECTION ( 'NONE',  ( 0.000000000000000000, -2.173523156925979552E-06, 0.9999999999976378895 ) ) ;
#58362=CARTESIAN_POINT ( 'NONE',  ( 9.714863677370791706, 19.00186346016302608, -1.500000000000002220 ) ) ;
#58363=DIRECTION ( 'NONE',  ( -3.773278334444166432E-23, 1.000000000000000000, 0.000000000000000000 ) ) ;
#58364=CARTESIAN_POINT ( 'NONE',  ( -51.95144507529695233, -25.20650842489795451, 6.812665538484691474 ) ) ;
#58365=CARTESIAN_POINT ( 'NONE',  ( -64.51565993021132783, -23.73791477778911840, 11.05961554403170766 ) ) ;
#58367=CARTESIAN_POINT ( 'NONE',  ( 8.141615846073909424, -21.09679883994429161, -1.500000000000002220 ) ) ;
#58371=CARTESIAN_POINT ( 'NONE',  ( -65.52287095715006160, -29.50248528299804818, 1.056150453629036701 ) ) ;
#58372=CARTESIAN_POINT ( 'NONE',  ( -79.62361060721978845, -24.65952944569304606, 1.056160979905701902 ) ) ;
#58373=CARTESIAN_POINT ( 'NONE',  ( -0.9724026449420489771, -19.73431249065222204, 11.49999999999999645 ) ) ;
#58375=CARTESIAN_POINT ( 'NONE',  ( -32.07722060962684196, -25.25098752628340293, 6.467533449461289941 ) ) ;
#58377=LINE ( 'NONE', #51253, #79811 ) ;
#58378=CARTESIAN_POINT ( 'NONE',  ( -29.66447556523817397, -24.60094274054533159, 3.393818988263333392 ) ) ;
#58381=CARTESIAN_POINT ( 'NONE',  ( 18.49883484089910723, -11.16122333755292750, -1.500000000000002220 ) ) ;
#58384=CARTESIAN_POINT ( 'NONE',  ( -70.55620429048339304, -25.00158670708909625, 2.256160236439166855 ) ) ;
#58385=EDGE_CURVE ( 'NONE', #11431, #69290, #23799, .T. ) ;
#58388=CARTESIAN_POINT ( 'NONE',  ( -3.504374479207110316, 19.46862825742285708, 11.49999999999998934 ) ) ;
#58389=VERTEX_POINT ( 'NONE', #46633 ) ;
#58391=CARTESIAN_POINT ( 'NONE',  ( 13.48481281434462531, 15.16087405922196041, 11.49999999999999645 ) ) ;
#58393=VECTOR ( 'NONE', #25469, 1000.000000000000114 ) ;
#58394=CARTESIAN_POINT ( 'NONE',  ( -29.81175120719462157, -29.50249373072461623, 4.942801737957442931 ) ) ;
#58395=ORIENTED_EDGE ( 'NONE', *, *, #79560, .T. ) ;
#58396=LINE ( 'NONE', #97922, #99295 ) ;
#58398=CARTESIAN_POINT ( 'NONE',  ( -75.52287095715011844, -23.48783264082477373, -1.443836473390087694 ) ) ;
#58399=CARTESIAN_POINT ( 'NONE',  ( -103.6228709571500985, -24.50321055353806443, 9.387540953477532923 ) ) ;
#58400=CARTESIAN_POINT ( 'NONE',  ( -50.40445135320379677, -25.12298712672050982, 7.101635559041870494 ) ) ;
#58401=CARTESIAN_POINT ( 'NONE',  ( 11.63622169266987783, 16.31392799894670631, 11.49999999999998934 ) ) ;
#58402=ADVANCED_FACE ( 'NONE', ( #76057 ), #100379, .T. ) ;
#58403=CARTESIAN_POINT ( 'NONE',  ( -54.52287095715006870, -29.50248528299804818, 1.056150453629033370 ) ) ;
#58405=ADVANCED_FACE ( 'NONE', ( #29892 ), #44626, .F. ) ;
#58406=VECTOR ( 'NONE', #46325, 1000.000000000000114 ) ;
#58409=DIRECTION ( 'NONE',  ( 3.773278334444166432E-23, -1.000000000000000000, 0.000000000000000000 ) ) ;
#58413=B_SPLINE_CURVE_WITH_KNOTS ( 'NONE', 3,
 ( #1293, #63200, #56591, #94628, #64209, #95133 ),
 .UNSPECIFIED., .F., .F.,
 ( 4, 2, 4 ),
 ( 1.570887131794176733E-05, 0.001396322306279758037, 0.002776935741241574537 ),
 .UNSPECIFIED. ) ;
#58417=CARTESIAN_POINT ( 'NONE',  ( -50.78266031332166364, -25.23256535379771037, 6.480020017899467355 ) ) ;
#58419=CARTESIAN_POINT ( 'NONE',  ( -9.641467040090685003, 17.89903724589931855, -1.500000000000002220 ) ) ;
#58421=CARTESIAN_POINT ( 'NONE',  ( -12.73177969873712279, -19.06072230859735939, -1.500000000000002220 ) ) ;
#58423=CARTESIAN_POINT ( 'NONE',  ( -32.62929916188119250, -24.51314013834315375, 0.6176544820404111791 ) ) ;
#58425=CARTESIAN_POINT ( 'NONE',  ( -108.5228709571501184, -23.96177878511310055, 10.65340807706329684 ) ) ;
#58427=CARTESIAN_POINT ( 'NONE',  ( -49.51155500790866171, -25.12215341870864194, 6.743855441649687421 ) ) ;
#58428=CARTESIAN_POINT ( 'NONE',  ( -74.52287095715007581, -23.47593901973090169, -1.443836447538996870 ) ) ;
#58429=CARTESIAN_POINT ( 'NONE',  ( 12.09327641706010326, 17.40255341615222306, 11.49999999999999645 ) ) ;
#58430=CARTESIAN_POINT ( 'NONE',  ( 15.99899278244174639, -15.33069297701436184, 11.49999999999998934 ) ) ;
#58431=CARTESIAN_POINT ( 'NONE',  ( 19.85042311639309531, 5.490197614093233369, 11.49999999999998934 ) ) ;
#58432=VERTEX_POINT ( 'NONE', #38007 ) ;
#58433=CARTESIAN_POINT ( 'NONE',  ( -43.52287095715005449, -23.72747288104469732, -1.053458166803227680 ) ) ;
#58434=ORIENTED_EDGE ( 'NONE', *, *, #75831, .F. ) ;
#58437=VERTEX_POINT ( 'NONE', #67466 ) ;
#58438=VERTEX_POINT ( 'NONE', #98391 ) ;
#58439=ORIENTED_EDGE ( 'NONE', *, *, #67383, .T. ) ;
#58440=CARTESIAN_POINT ( 'NONE',  ( -83.62287095715007013, -24.34917612406838927, 0.1852690917426621231 ) ) ;
#58441=CARTESIAN_POINT ( 'NONE',  ( -46.52287095715006160, -24.64898659630367561, 1.056161002820821038 ) ) ;
#58443=CARTESIAN_POINT ( 'NONE',  ( 14.74948264216024008, 14.65492983226340407, -1.500000000000002220 ) ) ;
#58444=B_SPLINE_CURVE_WITH_KNOTS ( 'NONE', 3,
 ( #4289, #26627, #57588, #26121, #88525, #11891 ),
 .UNSPECIFIED., .F., .F.,
 ( 4, 2, 4 ),
 ( 0.000000000000000000, 0.001380901958385390062, 0.002761803916770780125 ),
 .UNSPECIFIED. ) ;
#58445=CARTESIAN_POINT ( 'NONE',  ( -1.268225406894735396, -21.67698866206750097, 11.49999999999999645 ) ) ;
#58447=DIRECTION ( 'NONE',  ( -3.773278334453079618E-23, 0.9999999999976377785, 2.173523156925979975E-06 ) ) ;
#58448=CARTESIAN_POINT ( 'NONE',  ( -115.5872436222452535, -24.92564183028979130, 1.928384488918252870 ) ) ;
#58449=CARTESIAN_POINT ( 'NONE',  ( 17.77913403553526805, 13.70458096452923691, 11.49999999999998934 ) ) ;
#58450=B_SPLINE_CURVE_WITH_KNOTS ( 'NONE', 3,
 ( #39834, #48464, #79394, #9883, #95125, #87519 ),
 .UNSPECIFIED., .F., .F.,
 ( 4, 2, 4 ),
 ( 6.391158118963033063E-06, 0.001387004593080781159, 0.002767618028042598960 ),
 .UNSPECIFIED. ) ;
#58452=CARTESIAN_POINT ( 'NONE',  ( -65.56866842408459206, -23.48783264082477018, -1.443836473390096353 ) ) ;
#58455=CARTESIAN_POINT ( 'NONE',  ( -85.52287095715004739, -24.99132157543166954, 2.256160258750667502 ) ) ;
#58458=VECTOR ( 'NONE', #3428, 1000.000000000000114 ) ;
#58460=ORIENTED_EDGE ( 'NONE', *, *, #75886, .T. ) ;
#58461=CARTESIAN_POINT ( 'NONE',  ( -3.120219904758775975, 21.05623772282662998, -1.500000000000002220 ) ) ;
#58462=VERTEX_POINT ( 'NONE', #28894 ) ;
#58463=CARTESIAN_POINT ( 'NONE',  ( -89.81226385320383088, -29.50249691823240994, 6.409318347766594037 ) ) ;
#58464=CARTESIAN_POINT ( 'NONE',  ( 21.05697796394607835, 5.830696701215154043, -1.500000000000002220 ) ) ;
#58465=PLANE ( 'NONE',  #91862 ) ;
#58466=CARTESIAN_POINT ( 'NONE',  ( 9.008567143757492346, 20.83016157428379955, -1.500000000000002220 ) ) ;
#58469=CARTESIAN_POINT ( 'NONE',  ( 1.885617179787854036, 21.85875792104173598, -1.500000000000002220 ) ) ;
#58473=CARTESIAN_POINT ( 'NONE',  ( -121.5895376238167103, -23.47593901973091235, -1.443836447538997536 ) ) ;
#58475=CARTESIAN_POINT ( 'NONE',  ( -99.62287095715002749, -23.95044443724991012, 10.65354141964649592 ) ) ;
#58477=ORIENTED_EDGE ( 'NONE', *, *, #87332, .F. ) ;
#58481=CARTESIAN_POINT ( 'NONE',  ( 19.98919582620916913, -7.218065965386815996, 11.49999999999998934 ) ) ;
#58482=CARTESIAN_POINT ( 'NONE',  ( -112.6317001763909929, -23.48783264082478794, -1.443836473390061492 ) ) ;
#58484=CARTESIAN_POINT ( 'NONE',  ( -85.53959574234744423, -24.92564183028979485, 1.928384488918252204 ) ) ;
#58485=DIRECTION ( 'NONE',  ( -3.773278334444166432E-23, 1.000000000000000000, 0.000000000000000000 ) ) ;
#58488=EDGE_CURVE ( 'NONE', #88020, #7140, #60370, .T. ) ;
#58489=CARTESIAN_POINT ( 'NONE',  ( -18.05301863641116000, -7.546005365994440162, 11.49999999999999645 ) ) ;
#58490=CARTESIAN_POINT ( 'NONE',  ( -58.62287095715004170, -24.35013146730203459, 9.818937971375111928 ) ) ;
#58491=EDGE_CURVE ( 'NONE', #58657, #53793, #21266, .T. ) ;
#58492=FACE_OUTER_BOUND ( 'NONE', #87366, .T. ) ;
#58493=VERTEX_POINT ( 'NONE', #61361 ) ;
#58494=EDGE_CURVE ( 'NONE', #89121, #7353, #63732, .T. ) ;
#58496=CARTESIAN_POINT ( 'NONE',  ( -99.55523467558795403, -25.31557864785565926, 4.972803384765369650 ) ) ;
#58498=FACE_OUTER_BOUND ( 'NONE', #4209, .T. ) ;
#58499=ADVANCED_FACE ( 'NONE', ( #70462 ), #40006, .T. ) ;
#58500=CARTESIAN_POINT ( 'NONE',  ( -62.62287095715004881, -23.48783264082478794, -1.443836473390068820 ) ) ;
#58501=CARTESIAN_POINT ( 'NONE',  ( 19.63295818312489871, -1.572306604260808260, -1.500000000000002220 ) ) ;
#58504=DIRECTION ( 'NONE',  ( -3.773278334453079030E-23, 0.9999999999976377785, 2.173523156925979128E-06 ) ) ;
#58509=CARTESIAN_POINT ( 'NONE',  ( -104.6228709571500559, -23.47593901973091235, -1.443836447539001089 ) ) ;
#58510=CARTESIAN_POINT ( 'NONE',  ( -118.5530130326516627, -24.51314013834317151, 0.6176544820404247238 ) ) ;
#58514=CARTESIAN_POINT ( 'NONE',  ( -14.87316555497233495, -13.31901947624662519, -1.500000000000002220 ) ) ;
#58515=CARTESIAN_POINT ( 'NONE',  ( -0.04339346789285819517, -22.48823745777612970, 1.345137965621359122 ) ) ;
#58516=CARTESIAN_POINT ( 'NONE',  ( 15.68239283413728735, 12.23493734220040530, -1.500000000000002220 ) ) ;
#58517=ORIENTED_EDGE ( 'NONE', *, *, #16773, .F. ) ;
#58518=CARTESIAN_POINT ( 'NONE',  ( -116.6228709571500275, -23.47596703998600631, 11.44779298504227860 ) ) ;
#58522=CARTESIAN_POINT ( 'NONE',  ( -49.62287095715004881, -23.96177878511307568, 10.65340807706329684 ) ) ;
#58527=CARTESIAN_POINT ( 'NONE',  ( -127.5550744602278428, -24.65952944569305316, 1.056160979905707009 ) ) ;
#58529=CARTESIAN_POINT ( 'NONE',  ( -5.512817753899047268, 19.46650688538001361, -1.500000000000002220 ) ) ;
#58530=LINE ( 'NONE', #21431, #19287 ) ;
#58533=ADVANCED_FACE ( 'NONE', ( #40521 ), #57960, .T. ) ;
#58534=ORIENTED_EDGE ( 'NONE', *, *, #49910, .T. ) ;
#58538=CARTESIAN_POINT ( 'NONE',  ( -18.81522532469529452, 6.996975221643539911, -1.500000000000002220 ) ) ;
#58539=CARTESIAN_POINT ( 'NONE',  ( 21.04674311342985860, -0.3259866984596996864, 11.49999999999999645 ) ) ;
#58540=CARTESIAN_POINT ( 'NONE',  ( -29.17217916550134404, -25.16101538479635025, 6.097600585202582302 ) ) ;
#58541=CARTESIAN_POINT ( 'NONE',  ( -70.54349239131259708, -24.52399227489127043, 9.353111116836524630 ) ) ;
#58542=CARTESIAN_POINT ( 'NONE',  ( -17.20036718215007099, 13.84871166177648583, -1.500000000000002220 ) ) ;
#58544=CARTESIAN_POINT ( 'NONE',  ( -39.48225211724125927, -25.27805969471785019, 4.451013812573177297 ) ) ;
#58545=CARTESIAN_POINT ( 'NONE',  ( -87.62287095715001328, -23.48786465467241769, 11.44779295918254114 ) ) ;
#58546=CARTESIAN_POINT ( 'NONE',  ( -50.30027857337484676, -25.18440102389800828, 3.296100527055671581 ) ) ;
#58548=CARTESIAN_POINT ( 'NONE',  ( -74.52287095715007581, -23.47593901973090169, -1.443836447538996870 ) ) ;
#58550=ORIENTED_EDGE ( 'NONE', *, *, #59769, .F. ) ;
#58551=ORIENTED_EDGE ( 'NONE', *, *, #35349, .T. ) ;
#58553=CARTESIAN_POINT ( 'NONE',  ( -124.6228709571500701, -23.47596703998600631, 11.44779298504227860 ) ) ;
#58555=CARTESIAN_POINT ( 'NONE',  ( -15.41819309731374510, 13.62919173607049927, -1.500000000000002220 ) ) ;
#58556=CARTESIAN_POINT ( 'NONE',  ( 16.61904782137575154, -13.72857183568914685, 11.49999999999999645 ) ) ;
#58559=CARTESIAN_POINT ( 'NONE',  ( -53.52287095715006870, -29.50250243563736774, 8.947779886222146928 ) ) ;
#58561=CARTESIAN_POINT ( 'NONE',  ( -7.140196579304709523, 21.16591527347414115, 11.49999999999998934 ) ) ;
#58563=CARTESIAN_POINT ( 'NONE',  ( -76.62287095715007013, -29.50248528299804818, 1.056150453629038477 ) ) ;
#58565=DIRECTION ( 'NONE',  ( -3.773278334453080206E-23, 0.9999999999976377785, 2.173523156925979975E-06 ) ) ;
#58567=CARTESIAN_POINT ( 'NONE',  ( 17.12911088700535700, -11.98135219954639830, -1.500000000000002220 ) ) ;
#58568=ORIENTED_EDGE ( 'NONE', *, *, #87437, .F. ) ;
#58569=CARTESIAN_POINT ( 'NONE',  ( -92.62287095715005592, -24.65952944569304606, 1.056160979905700348 ) ) ;
#58570=VERTEX_POINT ( 'NONE', #23773 ) ;
#58571=VERTEX_POINT ( 'NONE', #54748 ) ;
#58572=CARTESIAN_POINT ( 'NONE',  ( -100.5114778985442570, -24.40133493613050319, 9.663955038902802386 ) ) ;
#58573=CARTESIAN_POINT ( 'NONE',  ( -15.95541298346445735, 13.85296639876547076, -1.500000000000002220 ) ) ;
#58574=VERTEX_POINT ( 'NONE', #86678 ) ;
#58575=CARTESIAN_POINT ( 'NONE',  ( -37.58953762381673869, -23.47596703998600276, 11.44779298504227505 ) ) ;
#58576=CARTESIAN_POINT ( 'NONE',  ( -29.62287095715004881, -24.57400415421967566, 8.947790463233827651 ) ) ;
#58577=DIRECTION ( 'NONE',  ( 0.000000000000000000, 2.173523156925980399E-06, -0.9999999999976378895 ) ) ;
#58579=CARTESIAN_POINT ( 'NONE',  ( -49.37981359748505383, -25.18092312992202508, 3.262587406134465073 ) ) ;
#58580=CARTESIAN_POINT ( 'NONE',  ( 8.489507321284875729, -19.98171680480944445, -1.500000000000002220 ) ) ;
#58581=CARTESIAN_POINT ( 'NONE',  ( -107.5895376238167387, -23.48783264082479150, -1.443836473390060382 ) ) ;
#58582=CARTESIAN_POINT ( 'NONE',  ( 0.6114060112162268412, -22.25658958135186793, 11.49999999999999645 ) ) ;
#58584=CARTESIAN_POINT ( 'NONE',  ( -50.61185169649064619, -25.24728727379448046, 5.215441029265593720 ) ) ;
#58587=ORIENTED_EDGE ( 'NONE', *, *, #88775, .F. ) ;
#58588=CARTESIAN_POINT ( 'NONE',  ( -99.52287095715006160, -24.65952944569304961, 1.056160979905702346 ) ) ;
#58589=ORIENTED_EDGE ( 'NONE', *, *, #18835, .T. ) ;
#58590=ORIENTED_EDGE ( 'NONE', *, *, #28304, .T. ) ;
#58593=CARTESIAN_POINT ( 'NONE',  ( -63.58953762381673869, -24.65952944569304250, 1.056160979905695907 ) ) ;
#58594=CARTESIAN_POINT ( 'NONE',  ( -107.5228709571501184, -24.34917612407031129, 0.1852690917477051169 ) ) ;
#58598=CARTESIAN_POINT ( 'NONE',  ( 4.481524277812761525, 18.85844072219565604, 11.49999999999999645 ) ) ;
#58599=CARTESIAN_POINT ( 'NONE',  ( -115.5228709571500758, -23.85229601348997264, 10.88205029486208630 ) ) ;
#58600=CARTESIAN_POINT ( 'NONE',  ( 1.786768808452938950, -22.39398889530128756, -1.500000000000002220 ) ) ;
#58602=CARTESIAN_POINT ( 'NONE',  ( -45.52287095715007581, -23.47593901973090169, -1.443836447538997092 ) ) ;
#58604=LINE ( 'NONE', #51991, #73321 ) ;
#58606=ADVANCED_FACE ( 'NONE', ( #90176 ), #22346, .T. ) ;
#58607=CARTESIAN_POINT ( 'NONE',  ( -97.24578741328294029, -24.82935162629097192, 1.633150109380539172 ) ) ;
#58608=VECTOR ( 'NONE', #83194, 1000.000000000000114 ) ;
#58609=CARTESIAN_POINT ( 'NONE',  ( 7.829539893445508270, 17.95258299782629408, 11.49999999999998934 ) ) ;
#58611=PLANE ( 'NONE',  #41287 ) ;
#58614=CARTESIAN_POINT ( 'NONE',  ( -18.46100929034391314, -11.06139713797464985, 11.49999999999998934 ) ) ;
#58615=DIRECTION ( 'NONE',  ( -3.773278334453079618E-23, 0.9999999999976377785, 2.173523156925979975E-06 ) ) ;
#58617=CARTESIAN_POINT ( 'NONE',  ( -119.5562042904834072, -23.47596703998600631, 11.44779298504227683 ) ) ;
#58618=CARTESIAN_POINT ( 'NONE',  ( -59.62287095715004170, -24.65952944569304606, 1.056160979905694131 ) ) ;
#58619=CARTESIAN_POINT ( 'NONE',  ( -77.62287095715007013, -23.73934037231757443, 11.05740245334329153 ) ) ;
#58620=CARTESIAN_POINT ( 'NONE',  ( 13.47786528765806580, -18.65256936556403744, -1.500000000000002220 ) ) ;
#58623=CARTESIAN_POINT ( 'NONE',  ( -49.63343115848626752, -24.34968618360933590, 0.1864209137778799763 ) ) ;
#58624=CARTESIAN_POINT ( 'NONE',  ( 2.654622155064554789, -19.98241913370796041, 11.49999999999999645 ) ) ;
#58625=CARTESIAN_POINT ( 'NONE',  ( -109.1652331756773862, -25.10927527791083946, 3.437502883451723612 ) ) ;
#58626=CARTESIAN_POINT ( 'NONE',  ( -74.52287095715007581, -29.50250786944525672, 11.44777988621623699 ) ) ;
#58627=CARTESIAN_POINT ( 'NONE',  ( -46.52287095715005449, -23.96127896941631619, -0.6493128931038071316 ) ) ;
#58629=ADVANCED_FACE ( 'NONE', ( #33264 ), #17545, .F. ) ;
#58630=LINE ( 'NONE', #89575, #15412 ) ;
#58631=CARTESIAN_POINT ( 'NONE',  ( 13.99221305778824487, -14.08248706038611964, -1.500000000000002220 ) ) ;
#58632=CARTESIAN_POINT ( 'NONE',  ( -125.5228709571500616, -23.47596703998600631, 11.44779298504227683 ) ) ;
#58633=CARTESIAN_POINT ( 'NONE',  ( 3.669390655483735220, -19.36157329643844704, -1.500000000000002220 ) ) ;
#58634=CARTESIAN_POINT ( 'NONE',  ( -42.48188582566654503, -24.65952944569304606, 1.056160979905694353 ) ) ;
#58635=B_SPLINE_CURVE_WITH_KNOTS ( 'NONE', 3,
 ( #59006, #98035, #36650, #60995 ),
 .UNSPECIFIED., .F., .F.,
 ( 4, 4 ),
 ( 0.000000000000000000, 9.999999999998897304E-05 ),
 .UNSPECIFIED. ) ;
#58636=CARTESIAN_POINT ( 'NONE',  ( -110.5228709571500616, -23.47596703998600631, 11.44779298504228038 ) ) ;
#58637=CARTESIAN_POINT ( 'NONE',  ( -111.5228709571500190, -23.48783264082477018, -1.443836473390084585 ) ) ;
#58638=CARTESIAN_POINT ( 'NONE',  ( 19.46067915675286386, 6.892634557253153105, 11.49999999999999645 ) ) ;
#58639=CARTESIAN_POINT ( 'NONE',  ( -120.5520473220775983, -25.00158670708911046, 2.256160236439219702 ) ) ;
#58640=CARTESIAN_POINT ( 'NONE',  ( -20.89466310375201985, -8.809181082428260368, 11.49999999999999645 ) ) ;
#58642=ORIENTED_EDGE ( 'NONE', *, *, #82475, .T. ) ;
#58644=CARTESIAN_POINT ( 'NONE',  ( -93.52287095715006160, -23.47596703998600631, 11.44779298504228393 ) ) ;
#58646=CARTESIAN_POINT ( 'NONE',  ( -98.62287095715004170, -24.65952944569304606, 1.056160979905700792 ) ) ;
#58647=CARTESIAN_POINT ( 'NONE',  ( -56.52287095715008292, -24.35013146730203815, 9.818937971375104823 ) ) ;
#58649=VERTEX_POINT ( 'NONE', #77922 ) ;
#58650=DIRECTION ( 'NONE',  ( -3.773278334453079030E-23, 0.9999999999976377785, 2.173523156925979128E-06 ) ) ;
#58651=CARTESIAN_POINT ( 'NONE',  ( 9.198035947750891950, -20.93187084735588144, -1.500000000000002220 ) ) ;
#58653=CARTESIAN_POINT ( 'NONE',  ( 21.52761780497506905, -1.784033869580059939, -1.500000000000002220 ) ) ;
#58654=CARTESIAN_POINT ( 'NONE',  ( -113.5205645610192562, -23.73791477778911840, 11.05961554403170233 ) ) ;
#58655=DIRECTION ( 'NONE',  ( -3.773278334453079618E-23, 0.9999999999976377785, 2.173523156925979975E-06 ) ) ;
#58656=CARTESIAN_POINT ( 'NONE',  ( 22.54279463279464579, 0.6884863543687869125, 11.49999999999999645 ) ) ;
#58657=VERTEX_POINT ( 'NONE', #48007 ) ;
#58658=CARTESIAN_POINT ( 'NONE',  ( -28.94430083015267030, -25.04003078313435537, 3.099314279037052700 ) ) ;
#58660=CARTESIAN_POINT ( 'NONE',  ( 21.99661117994144988, 0.4758108284031232760, -1.500000000000002220 ) ) ;
#58662=CARTESIAN_POINT ( 'NONE',  ( -29.24615158708846963, -25.21724433438351198, 5.024434671431828647 ) ) ;
#58663=ORIENTED_EDGE ( 'NONE', *, *, #90335, .F. ) ;
#58665=EDGE_CURVE ( 'NONE', #18147, #61918, #74659, .T. ) ;
#58666=CARTESIAN_POINT ( 'NONE',  ( -47.55620429048338593, -23.47596703998600276, 11.44779298504227505 ) ) ;
#58667=ORIENTED_EDGE ( 'NONE', *, *, #69005, .F. ) ;
#58668=CARTESIAN_POINT ( 'NONE',  ( -45.52287095715007581, -23.47593901973090169, -1.443836447538997092 ) ) ;
#58669=ORIENTED_EDGE ( 'NONE', *, *, #68333, .T. ) ;
#58671=ORIENTED_EDGE ( 'NONE', *, *, #63686, .T. ) ;
#58672=CARTESIAN_POINT ( 'NONE',  ( -100.6228709571500559, -29.50249982740957577, 7.747779886224967605 ) ) ;
#58674=CARTESIAN_POINT ( 'NONE',  ( -57.53373409370878733, -24.65952944569304606, 1.056160979905698571 ) ) ;
#58675=CARTESIAN_POINT ( 'NONE',  ( 20.35419724272142616, 1.316291261081859787, -1.500000000000002220 ) ) ;
#58676=EDGE_CURVE ( 'NONE', #7077, #52807, #92809, .T. ) ;
#58677=ORIENTED_EDGE ( 'NONE', *, *, #80574, .F. ) ;
#58681=CARTESIAN_POINT ( 'NONE',  ( -97.52287095715007581, -24.33832256527048798, 0.1851278514138655906 ) ) ;
#58682=PLANE ( 'NONE',  #38265 ) ;
#58684=CARTESIAN_POINT ( 'NONE',  ( -75.48966160648491552, -25.00158670708910691, 2.256160236439223699 ) ) ;
#58685=CARTESIAN_POINT ( 'NONE',  ( -86.62287095715005592, -23.48786465467241413, 11.44779295918254469 ) ) ;
#58687=EDGE_LOOP ( 'NONE', ( #13726, #4522, #98499, #71149 ) ) ;
#58688=CARTESIAN_POINT ( 'NONE',  ( -8.119355292522030254, -19.11072509857415369, -1.500000000000002220 ) ) ;
#58692=ORIENTED_EDGE ( 'NONE', *, *, #63532, .F. ) ;
#58695=ORIENTED_EDGE ( 'NONE', *, *, #34378, .T. ) ;
#58697=CARTESIAN_POINT ( 'NONE',  ( -33.52287095715007581, -23.72773821059535848, 11.05748984161097681 ) ) ;
#58698=LINE ( 'NONE', #18135, #46462 ) ;
#58700=CARTESIAN_POINT ( 'NONE',  ( -43.50597321196386957, -23.96169478059712787, 10.65365249895718769 ) ) ;
#58701=CARTESIAN_POINT ( 'NONE',  ( 7.643743511751816655, -20.74876368896106271, 11.49999999999999645 ) ) ;
#58702=ORIENTED_EDGE ( 'NONE', *, *, #57595, .T. ) ;
#58703=CARTESIAN_POINT ( 'NONE',  ( -108.5890517283027918, -24.34968618360934300, 0.1864209137778971292 ) ) ;
#58704=CARTESIAN_POINT ( 'NONE',  ( -8.787219534579676861, -20.84281209399103929, -1.500000000000002220 ) ) ;
#58705=CARTESIAN_POINT ( 'NONE',  ( -115.5133545927454719, -25.00182538069147142, 7.747789668545041586 ) ) ;
#58707=ORIENTED_EDGE ( 'NONE', *, *, #21007, .T. ) ;
#58708=B_SPLINE_CURVE_WITH_KNOTS ( 'NONE', 3,
 ( #26703, #89598, #96219, #4373 ),
 .UNSPECIFIED., .F., .F.,
 ( 4, 4 ),
 ( 6.938893903907228378E-18, 8.001919664664916716E-05 ),
 .UNSPECIFIED. ) ;
#58711=B_SPLINE_CURVE_WITH_KNOTS ( 'NONE', 3,
 ( #98746, #96757, #20623, #51590, #58210, #89152 ),
 .UNSPECIFIED., .F., .F.,
 ( 4, 2, 4 ),
 ( 1.570887131794952276E-05, 0.001396322306279763675, 0.002776935741241577573 ),
 .UNSPECIFIED. ) ;
#58713=ORIENTED_EDGE ( 'NONE', *, *, #64730, .T. ) ;
#58714=CARTESIAN_POINT ( 'NONE',  ( -21.01389645921736360, -2.595061309317715281, -1.500000000000002220 ) ) ;
#58717=CARTESIAN_POINT ( 'NONE',  ( -19.27636426328722763, -11.15942449563467775, -1.500000000000002220 ) ) ;
#58721=CARTESIAN_POINT ( 'NONE',  ( -50.52287095715006160, -23.47596703998600631, 11.44779298504229104 ) ) ;
#58722=B_SPLINE_CURVE_WITH_KNOTS ( 'NONE', 3,
 ( #30089, #98098, #82384, #30590 ),
 .UNSPECIFIED., .F., .F.,
 ( 4, 4 ),
 ( 0.000000000000000000, 1.000000000000000000 ),
 .UNSPECIFIED. ) ;
#58725=CARTESIAN_POINT ( 'NONE',  ( 6.966380261627926451, -18.21767524041069564, 11.49999999999998934 ) ) ;
#58728=CARTESIAN_POINT ( 'NONE',  ( -19.34459864454321831, 9.218434461607088792, -1.500000000000002220 ) ) ;
#58729=CARTESIAN_POINT ( 'NONE',  ( -27.70544111104076990, -24.57999497002659695, 1.628749937114660540 ) ) ;
#58730=AXIS2_PLACEMENT_3D ( 'NONE', #75343, #5844, #29177 ) ;
#58731=EDGE_CURVE ( 'NONE', #31069, #86729, #27409, .T. ) ;
#58733=CARTESIAN_POINT ( 'NONE',  ( -34.52287095715006160, -23.47593901973090169, -1.443836447538997314 ) ) ;
#58734=CARTESIAN_POINT ( 'NONE',  ( 9.312063170398973355, -20.82641193498425025, -1.500000000000002220 ) ) ;
#58736=CARTESIAN_POINT ( 'NONE',  ( -107.6228709571500701, -29.50250243563736774, 8.947779886222136270 ) ) ;
#58737=CARTESIAN_POINT ( 'NONE',  ( -128.5228709571501611, -24.50216790748206108, 0.6166512839542577229 ) ) ;
#58738=CARTESIAN_POINT ( 'NONE',  ( 19.48829924427396421, 3.997931079995220127, 11.49999999999999645 ) ) ;
#58739=CARTESIAN_POINT ( 'NONE',  ( -104.6328447509342539, -23.73766607897670866, -1.055555164236450016 ) ) ;
#58740=CARTESIAN_POINT ( 'NONE',  ( -74.63881899433903300, -23.96169478059713498, 10.65365249895717881 ) ) ;
#58741=CARTESIAN_POINT ( 'NONE',  ( -48.56837829547282581, -23.48783264082477729, -1.443836473390069264 ) ) ;
#58742=EDGE_LOOP ( 'NONE', ( #12889, #16099, #47901, #10693 ) ) ;
#58743=EDGE_CURVE ( 'NONE', #94221, #23708, #24644, .T. ) ;
#58744=CARTESIAN_POINT ( 'NONE',  ( -25.53321154136338933, -24.92494999122525456, 4.756956508522131699 ) ) ;
#58745=CARTESIAN_POINT ( 'NONE',  ( -62.62287095715007723, -24.50321055353805022, 9.387540953477532923 ) ) ;
#58746=CARTESIAN_POINT ( 'NONE',  ( 10.00111611332133421, -19.26892646806700071, 11.49999999999998934 ) ) ;
#58747=CARTESIAN_POINT ( 'NONE',  ( -77.62287095715007013, -24.66019654487199730, 8.947790411086128159 ) ) ;
#58748=CARTESIAN_POINT ( 'NONE',  ( -1.979602623192304955, -19.45764201480039901, -1.500000000000002220 ) ) ;
#58751=ORIENTED_EDGE ( 'NONE', *, *, #5153, .T. ) ;
#58754=DIRECTION ( 'NONE',  ( -3.773278334453079030E-23, 0.9999999999976377785, 2.173523156925979128E-06 ) ) ;
#58755=CARTESIAN_POINT ( 'NONE',  ( -17.80769721941407369, -10.09151516499986734, 11.49999999999999645 ) ) ;
#58757=CARTESIAN_POINT ( 'NONE',  ( -61.25483432547240881, -25.20321001719939957, 6.713658772143283215 ) ) ;
#58758=AXIS2_PLACEMENT_3D ( 'NONE', #49144, #3462, #26784 ) ;
#58759=ORIENTED_EDGE ( 'NONE', *, *, #22888, .F. ) ;
#58761=CARTESIAN_POINT ( 'NONE',  ( -39.44687923781921057, -25.18431065692472259, 4.188173887285336683 ) ) ;
#58765=CARTESIAN_POINT ( 'NONE',  ( -98.62287095715007013, -23.47596703998600631, 11.44779298504227860 ) ) ;
#58766=ORIENTED_EDGE ( 'NONE', *, *, #19017, .F. ) ;
#58767=CARTESIAN_POINT ( 'NONE',  ( -80.96226385320385077, -25.14083923594767001, 2.947789366383926968 ) ) ;
#58768=EDGE_CURVE ( 'NONE', #16463, #4897, #4413, .T. ) ;
#58769=CARTESIAN_POINT ( 'NONE',  ( -18.14924840124409045, -14.16824886576183040, 11.49999999999999645 ) ) ;
#58770=CARTESIAN_POINT ( 'NONE',  ( 0.8422786845129024424, 22.77647355728978340, 11.49999999999998934 ) ) ;
#58771=CARTESIAN_POINT ( 'NONE',  ( -110.5193695319981657, -23.85049219812686161, 10.88485053497526778 ) ) ;
#58772=B_SPLINE_SURFACE_WITH_KNOTS ( 'NONE', 3, 3, ( 
 ( #23334, #47701, #71039, #47201 ),
 ( #54817, #63442, #17744, #92856 ),
 ( #48716, #63952, #1527, #78120 ),
 ( #71540, #39579, #24848, #24353 ),
 ( #79634, #86750, #78618, #23844 ),
 ( #77623, #9126, #8633, #2035 ),
 ( #25352, #17238, #10127, #70531 ),
 ( #48205, #1019, #79135, #9630 ),
 ( #31465, #94362, #93353, #70026 ),
 ( #85753, #55823, #41092, #54319 ) ),
 .UNSPECIFIED., .F., .F., .F.,
 ( 4, 3, 3, 4 ),
 ( 4, 4 ),
 ( 0.7022005934544807149, 0.7765311282028795059, 0.8508616629512784080, 0.9995227324480759901 ),
 ( 0.3495361808025915229, 0.3507572245070639250 ),
 .UNSPECIFIED. ) ;
#58773=CARTESIAN_POINT ( 'NONE',  ( -40.52287095715009002, -24.51163499207178376, 0.6490370598555547099 ) ) ;
#58774=CARTESIAN_POINT ( 'NONE',  ( -49.65519464679333339, -25.23424849805013892, 3.597430756124838869 ) ) ;
#58775=CARTESIAN_POINT ( 'NONE',  ( -50.62287095715005592, -25.00158670708909625, 2.256160236439165967 ) ) ;
#58776=CARTESIAN_POINT ( 'NONE',  ( -110.5947698665794832, -23.85016227208580375, -0.8807180028928308646 ) ) ;
#58777=CARTESIAN_POINT ( 'NONE',  ( 4.863445656156933694, -21.36585520573490626, 11.49999999999998934 ) ) ;
#58778=ADVANCED_FACE ( 'NONE', ( #54614 ), #61282, .T. ) ;
#58781=B_SPLINE_CURVE_WITH_KNOTS ( 'NONE', 3,
 ( #54194, #46075, #13602, #29835 ),
 .UNSPECIFIED., .F., .F.,
 ( 4, 4 ),
 ( 0.0001059329845610884477, 0.03369911402185697680 ),
 .UNSPECIFIED. ) ;
#58785=ORIENTED_EDGE ( 'NONE', *, *, #84803, .F. ) ;
#58786=CARTESIAN_POINT ( 'NONE',  ( -19.95082702767638239, -4.354873812894156870, -1.500000000000002220 ) ) ;
#58787=ORIENTED_EDGE ( 'NONE', *, *, #45300, .F. ) ;
#58789=ORIENTED_EDGE ( 'NONE', *, *, #17701, .F. ) ;
#58791=CARTESIAN_POINT ( 'NONE',  ( 22.66633601775066253, -4.223608244049824378, 11.49999999999998934 ) ) ;
#58792=CARTESIAN_POINT ( 'NONE',  ( -105.5895376238167387, -23.48783264082479150, -1.443836473390060160 ) ) ;
#58793=CARTESIAN_POINT ( 'NONE',  ( 3.706880958665978998, 19.89330832657401515, -1.500000000000002220 ) ) ;
#58795=ORIENTED_EDGE ( 'NONE', *, *, #31967, .T. ) ;
#58796=DIRECTION ( 'NONE',  ( -3.773278334453079618E-23, 0.9999999999976377785, 2.173523156925979975E-06 ) ) ;
#58798=CARTESIAN_POINT ( 'NONE',  ( -76.52287095715007581, -24.66019654487199730, 8.947790411086124607 ) ) ;
#58799=FACE_OUTER_BOUND ( 'NONE', #36744, .T. ) ;
#58800=CARTESIAN_POINT ( 'NONE',  ( -2.881439591185620319, 21.19155266312798958, 11.49999999999999645 ) ) ;
#58802=DIRECTION ( 'NONE',  ( 0.000000000000000000, 2.173523156925980399E-06, -0.9999999999976378895 ) ) ;
#58805=CARTESIAN_POINT ( 'NONE',  ( -21.31523168734759466, -6.469442287714795015, -1.500000000000002220 ) ) ;
#58806=CARTESIAN_POINT ( 'NONE',  ( -20.66316395829706209, -0.6310838753663271516, 11.49999999999998934 ) ) ;
#58808=B_SPLINE_CURVE_WITH_KNOTS ( 'NONE', 3,
 ( #98091, #51443, #13357, #44829, #82380, #67675, #29088, #28597, #59559, #90494 ),
 .UNSPECIFIED., .F., .F.,
 ( 4, 2, 2, 2, 4 ),
 ( 2.602085213965210642E-18, 0.0002772168619526806685, 0.0005544337239053587349, 0.0008316505858580367470, 0.001108867447810714868 ),
 .UNSPECIFIED. ) ;
#58809=ORIENTED_EDGE ( 'NONE', *, *, #43371, .T. ) ;
#58811=VERTEX_POINT ( 'NONE', #35777 ) ;
#58812=CARTESIAN_POINT ( 'NONE',  ( -81.52287095715006160, -24.34917612407036458, 0.1852690917478629073 ) ) ;
#58813=ORIENTED_EDGE ( 'NONE', *, *, #70993, .T. ) ;
#58814=CARTESIAN_POINT ( 'NONE',  ( 19.44712688777480736, 7.780496645421295376, -1.500000000000002220 ) ) ;
#58815=CARTESIAN_POINT ( 'NONE',  ( 20.57945552106664877, -7.502658216658728563, 11.49999999999999645 ) ) ;
#58816=B_SPLINE_CURVE_WITH_KNOTS ( 'NONE', 3,
 ( #76982, #51674, #98827, #22192 ),
 .UNSPECIFIED., .F., .F.,
 ( 4, 4 ),
 ( 0.000000000000000000, 9.999999999996123101E-05 ),
 .UNSPECIFIED. ) ;
#58818=CARTESIAN_POINT ( 'NONE',  ( -19.74168752133572724, 10.86179948771369297, 11.49999999999998934 ) ) ;
#58820=CARTESIAN_POINT ( 'NONE',  ( 20.88312143257166653, -1.666129412636018214, -1.500000000000002220 ) ) ;
#58821=B_SPLINE_CURVE_WITH_KNOTS ( 'NONE', 3,
 ( #75713, #30548, #45783, #90954 ),
 .UNSPECIFIED., .F., .F.,
 ( 4, 4 ),
 ( 1.387778780781445676E-17, 9.999999999998900014E-05 ),
 .UNSPECIFIED. ) ;
#58824=CARTESIAN_POINT ( 'NONE',  ( -119.5576586416463698, -23.48786465467241769, 11.44779295918253759 ) ) ;
#58829=VERTEX_POINT ( 'NONE', #81941 ) ;
#58830=ORIENTED_EDGE ( 'NONE', *, *, #100082, .F. ) ;
#58832=CARTESIAN_POINT ( 'NONE',  ( 15.63241172484657682, -14.69700884395465934, -1.500000000000002220 ) ) ;
#58833=VECTOR ( 'NONE', #65016, 1000.000000000000114 ) ;
#58835=VERTEX_POINT ( 'NONE', #64758 ) ;
#58836=CARTESIAN_POINT ( 'NONE',  ( -20.42954818520503935, 5.180689535515515587, -1.500000000000002220 ) ) ;
#58842=CARTESIAN_POINT ( 'NONE',  ( 14.53198226072946220, 16.64418356588832992, -1.500000000000002220 ) ) ;
#58843=VECTOR ( 'NONE', #73075, 1000.000000000000114 ) ;
#58845=CARTESIAN_POINT ( 'NONE',  ( -81.62360521410421654, -24.66019654487198665, 8.947790411086131712 ) ) ;
#58847=CARTESIAN_POINT ( 'NONE',  ( -51.93149462243456327, -25.31633352654386471, 6.174051004181417390 ) ) ;
#58850=CARTESIAN_POINT ( 'NONE',  ( 21.32124590881793225, -1.116183810207903804, 11.49999999999998934 ) ) ;
#58852=CARTESIAN_POINT ( 'NONE',  ( -90.25673798828883321, -25.26266127311082954, 3.981777872396911278 ) ) ;
#58853=EDGE_CURVE ( 'NONE', #36363, #2649, #86511, .T. ) ;
#58854=CARTESIAN_POINT ( 'NONE',  ( -64.49570014113403715, -24.51419770103158058, 9.386484678747169852 ) ) ;
#58856=CARTESIAN_POINT ( 'NONE',  ( -19.18631400275845422, -11.98935526391121087, -1.500000000000002220 ) ) ;
#58857=B_SPLINE_SURFACE_WITH_KNOTS ( 'NONE', 3, 3, ( 
 ( #93729, #69901, #46570, #30838 ),
 ( #54195, #47077, #61803, #48076 ),
 ( #85621, #1404, #16107, #77991 ),
 ( #54688, #23211, #24223, #56198 ),
 ( #38946, #79512, #8505, #25221 ),
 ( #39456, #92723, #63313, #70405 ),
 ( #55697, #62303, #892, #70913 ) ),
 .UNSPECIFIED., .F., .F., .F.,
 ( 4, 3, 4 ),
 ( 4, 4 ),
 ( 0.0004766839783843426618, 0.1029713700210909133, 0.2054660560637974753 ),
 ( 0.3795905586011096289, 0.3807784255434110698 ),
 .UNSPECIFIED. ) ;
#58861=CARTESIAN_POINT ( 'NONE',  ( -79.51716573576175051, -23.73766607897669800, -1.055555164236459564 ) ) ;
#58862=CARTESIAN_POINT ( 'NONE',  ( -5.448126336921106372, -18.99418723138115084, 11.49999999999999645 ) ) ;
#58863=CARTESIAN_POINT ( 'NONE',  ( -74.58953762381673869, -23.48783264082478794, -1.443836473390067265 ) ) ;
#58864=B_SPLINE_CURVE_WITH_KNOTS ( 'NONE', 3,
 ( #61962, #61464, #77159, #53848 ),
 .UNSPECIFIED., .F., .F.,
 ( 4, 4 ),
 ( 0.000000000000000000, 1.000000000000000000 ),
 .UNSPECIFIED. ) ;
#58866=CARTESIAN_POINT ( 'NONE',  ( -67.65233053103399641, -23.48783264082477018, -1.443836473390094799 ) ) ;
#58867=VERTEX_POINT ( 'NONE', #43395 ) ;
#58870=CARTESIAN_POINT ( 'NONE',  ( -29.54861811807234417, -25.26026587690250480, 3.015634576047991011 ) ) ;
#58872=CARTESIAN_POINT ( 'NONE',  ( -100.4426124108961176, -25.17353343843558378, 7.101635449178290926 ) ) ;
#58873=CARTESIAN_POINT ( 'NONE',  ( 18.49883484089910723, -11.16122333755292750, 11.49999999999998934 ) ) ;
#58874=CARTESIAN_POINT ( 'NONE',  ( -49.36186039879741116, -25.27517977621036849, 3.293514770891703858 ) ) ;
#58876=EDGE_CURVE ( 'NONE', #11406, #84649, #11574, .T. ) ;
#58877=PLANE ( 'NONE',  #85323 ) ;
#58878=CARTESIAN_POINT ( 'NONE',  ( -81.78239782233198696, -25.19580958332243981, 6.707330381882551151 ) ) ;
#58879=CARTESIAN_POINT ( 'NONE',  ( 14.45944668481935658, 13.51102189132778442, 11.49999999999998934 ) ) ;
#58882=CARTESIAN_POINT ( 'NONE',  ( 19.68333694646799614, 4.735253856516091098, 11.49999999999999645 ) ) ;
#58886=CARTESIAN_POINT ( 'NONE',  ( -37.52287095715006160, -23.73934037231756022, 11.05740245334329686 ) ) ;
#58888=CARTESIAN_POINT ( 'NONE',  ( -71.52287095715010423, -24.35013146730203815, 9.818937971375099494 ) ) ;
#58890=CARTESIAN_POINT ( 'NONE',  ( -50.54027953994811639, -25.12358199471872311, 7.098256093999977701 ) ) ;
#58891=CARTESIAN_POINT ( 'NONE',  ( 16.02535498940104830, 12.03463022438520191, 11.49999999999998934 ) ) ;
#58893=EDGE_LOOP ( 'NONE', ( #47654, #26575, #5607, #78736 ) ) ;
#58895=CARTESIAN_POINT ( 'NONE',  ( -32.62287095715004170, -23.96177878511308634, 10.65340807706331105 ) ) ;
#58896=CARTESIAN_POINT ( 'NONE',  ( -127.5228709571500616, -23.47593901973090524, -1.443836447538996204 ) ) ;
#58898=DIRECTION ( 'NONE',  ( -3.773278334453079030E-23, 0.9999999999976377785, 2.173523156925979128E-06 ) ) ;
#58899=FACE_OUTER_BOUND ( 'NONE', #97103, .T. ) ;
#58900=AXIS2_PLACEMENT_3D ( 'NONE', #1822, #77914, #310 ) ;
#58901=EDGE_CURVE ( 'NONE', #100062, #67442, #27666, .T. ) ;
#58902=EDGE_CURVE ( 'NONE', #61298, #69448, #50227, .T. ) ;
#58905=CARTESIAN_POINT ( 'NONE',  ( -14.66855384320708033, -14.05595220846724835, 11.49999999999998934 ) ) ;
#58908=CARTESIAN_POINT ( 'NONE',  ( 11.31314246093949727, 19.96360691973900359, 11.49999999999998934 ) ) ;
#58910=VERTEX_POINT ( 'NONE', #3346 ) ;
#58911=CARTESIAN_POINT ( 'NONE',  ( -108.5228709571501327, -24.51387760970724727, 9.387446482453400520 ) ) ;
#58912=B_SPLINE_CURVE_WITH_KNOTS ( 'NONE', 3,
 ( #47061, #93713, #24206, #93212 ),
 .UNSPECIFIED., .F., .F.,
 ( 4, 4 ),
 ( 0.000000000000000000, 9.999999999998897304E-05 ),
 .UNSPECIFIED. ) ;
#58913=LINE ( 'NONE', #98954, #22645 ) ;
#58914=CARTESIAN_POINT ( 'NONE',  ( -87.55620429048337883, -24.64898659630528854, 1.056161002820825923 ) ) ;
#58915=CARTESIAN_POINT ( 'NONE',  ( 4.903939382885006637, -20.63555827282145572, 11.49999999999999645 ) ) ;
#58918=CARTESIAN_POINT ( 'NONE',  ( -12.03526013704878039, -18.61824004984164560, 11.49999999999998934 ) ) ;
#58919=CARTESIAN_POINT ( 'NONE',  ( -11.90445915685808131, 16.78794160864392992, 11.49999999999998934 ) ) ;
#58922=ORIENTED_EDGE ( 'NONE', *, *, #8757, .T. ) ;
#58923=CARTESIAN_POINT ( 'NONE',  ( -57.52287095715005449, -29.50250243563736774, 8.947779886222145151 ) ) ;
#58924=LINE ( 'NONE', #49325, #92344 ) ;
#58925=ORIENTED_EDGE ( 'NONE', *, *, #41518, .F. ) ;
#58926=ORIENTED_EDGE ( 'NONE', *, *, #39031, .F. ) ;
#58929=CARTESIAN_POINT ( 'NONE',  ( -28.60235697241663999, -23.80516273491463508, 10.65365253163527015 ) ) ;
#58931=CARTESIAN_POINT ( 'NONE',  ( -18.78340662496949776, 8.880393494302802893, -1.500000000000002220 ) ) ;
#58932=CARTESIAN_POINT ( 'NONE',  ( 8.489507321284875729, -19.98171680480944445, 11.49999999999999645 ) ) ;
#58935=CARTESIAN_POINT ( 'NONE',  ( -40.33243357995862510, -25.18556298990670683, 3.298389014606699643 ) ) ;
#58939=CARTESIAN_POINT ( 'NONE',  ( -22.05133119090760019, 4.102169094691678453, 11.49999999999998934 ) ) ;
#58941=EDGE_CURVE ( 'NONE', #18541, #32116, #29150, .T. ) ;
#58942=CARTESIAN_POINT ( 'NONE',  ( -41.52287095715006870, -24.64898659630528144, 1.056161002820819261 ) ) ;
#58943=CARTESIAN_POINT ( 'NONE',  ( -34.62287095715007013, -23.47596703998600276, 11.44779298504227505 ) ) ;
#58944=VERTEX_POINT ( 'NONE', #83936 ) ;
#58947=B_SPLINE_CURVE_WITH_KNOTS ( 'NONE', 3,
 ( #65681, #50433, #4756, #35709, #27093, #3274 ),
 .UNSPECIFIED., .F., .F.,
 ( 4, 2, 4 ),
 ( 1.570755371634131319E-05, 0.001396183895866090138, 0.002776660238015839048 ),
 .UNSPECIFIED. ) ;
#58951=ORIENTED_EDGE ( 'NONE', *, *, #5597, .F. ) ;
#58952=DIRECTION ( 'NONE',  ( 0.000000000000000000, -0.9999999999976377785, -2.173523156925979128E-06 ) ) ;
#58954=CARTESIAN_POINT ( 'NONE',  ( 20.49606604269246546, -5.804284187783010474, -1.500000000000002220 ) ) ;
#58957=CARTESIAN_POINT ( 'NONE',  ( 13.92123049006271707, -16.85212209846622855, -1.500000000000002220 ) ) ;
#58958=CARTESIAN_POINT ( 'NONE',  ( -38.52287095715006160, -24.33927499327854349, 9.819080762295811837 ) ) ;
#58959=CARTESIAN_POINT ( 'NONE',  ( 19.36006514395606004, 11.85157241509795512, -1.500000000000002220 ) ) ;
#58960=CARTESIAN_POINT ( 'NONE',  ( -41.09701627025020088, -25.28892465612891627, 3.494173594328332300 ) ) ;
#58962=CARTESIAN_POINT ( 'NONE',  ( -19.33260374144687077, -10.33727041909969380, -1.500000000000002220 ) ) ;
#58963=CARTESIAN_POINT ( 'NONE',  ( -66.62287095715002749, -23.73907113216991860, -1.053371485793230811 ) ) ;
#58964=VERTEX_POINT ( 'NONE', #22017 ) ;
#58965=B_SPLINE_CURVE_WITH_KNOTS ( 'NONE', 3,
 ( #43301, #66158, #96085, #97073, #79846, #11834 ),
 .UNSPECIFIED., .F., .F.,
 ( 4, 2, 4 ),
 ( 0.000000000000000000, 0.001380764517853248817, 0.002761529035706497635 ),
 .UNSPECIFIED. ) ;
#58966=CARTESIAN_POINT ( 'NONE',  ( -122.5906892354238806, -23.96169478059714564, 10.65365249895717170 ) ) ;
#58967=DIRECTION ( 'NONE',  ( -3.773278334453080206E-23, 0.9999999999976377785, 2.173523156925979975E-06 ) ) ;
#58969=ADVANCED_FACE ( 'NONE', ( #6315 ), #10933, .T. ) ;
#58971=CARTESIAN_POINT ( 'NONE',  ( -49.52287095715006160, -23.48786465467241769, 11.44779295918255002 ) ) ;
#58972=DIRECTION ( 'NONE',  ( -3.773278334453079618E-23, 0.9999999999976377785, 2.173523156925979975E-06 ) ) ;
#58973=CARTESIAN_POINT ( 'NONE',  ( -10.23455669472452101, -23.17852390460462786, 1.363349870542264863 ) ) ;
#58974=CARTESIAN_POINT ( 'NONE',  ( -20.53569570583907122, -5.550916044964551155, 11.49999999999998934 ) ) ;
#58975=CARTESIAN_POINT ( 'NONE',  ( -112.5891746945082446, -24.34968618360934656, 0.1864209137779000991 ) ) ;
#58976=CARTESIAN_POINT ( 'NONE',  ( -26.09636659181000695, -24.75186549494400623, 4.940288025096378099 ) ) ;
#58977=EDGE_CURVE ( 'NONE', #75868, #7254, #9059, .T. ) ;
#58978=FACE_OUTER_BOUND ( 'NONE', #96611, .T. ) ;
#58979=CARTESIAN_POINT ( 'NONE',  ( -68.54060897849606704, -24.51314013834315375, 0.6176544820404119562 ) ) ;
#58980=B_SPLINE_CURVE_WITH_KNOTS ( 'NONE', 3,
 ( #30608, #83395, #21484, #99603 ),
 .UNSPECIFIED., .F., .F.,
 ( 4, 4 ),
 ( 0.000000000000000000, 9.999999999998900014E-05 ),
 .UNSPECIFIED. ) ;
#58981=AXIS2_PLACEMENT_3D ( 'NONE', #85689, #48649, #55757 ) ;
#58983=CARTESIAN_POINT ( 'NONE',  ( -117.6294113641524604, -23.48786465467241769, 11.44779295918253581 ) ) ;
#58984=EDGE_LOOP ( 'NONE', ( #35710, #76382, #53181, #83496 ) ) ;
#58985=CARTESIAN_POINT ( 'NONE',  ( -12.82114019720147802, -14.77593736753402709, 11.49999999999999645 ) ) ;
#58986=FACE_OUTER_BOUND ( 'NONE', #71802, .T. ) ;
#58988=CARTESIAN_POINT ( 'NONE',  ( -28.89879952236138294, -24.84188620179533302, 7.830688885502556928 ) ) ;
#58989=EDGE_LOOP ( 'NONE', ( #44019, #48286, #38601, #15756 ) ) ;
#58990=EDGE_CURVE ( 'NONE', #82250, #76858, #36913, .T. ) ;
#58992=CARTESIAN_POINT ( 'NONE',  ( -99.30277203926080176, -25.31439712689208577, 6.024134105486370849 ) ) ;
#58993=CARTESIAN_POINT ( 'NONE',  ( -31.62287095715005236, -23.94994826722514958, -0.6494450866351750840 ) ) ;
#58994=ADVANCED_FACE ( 'NONE', ( #12918 ), #7302, .T. ) ;
#58995=CARTESIAN_POINT ( 'NONE',  ( -106.5228709571500616, -23.73907113216990794, -1.053371485793244577 ) ) ;
#58996=CARTESIAN_POINT ( 'NONE',  ( 19.47230031930329730, 2.946587627359682493, -1.500000000000002220 ) ) ;
#58999=B_SPLINE_CURVE_WITH_KNOTS ( 'NONE', 3,
 ( #34077, #65050, #95967, #86189 ),
 .UNSPECIFIED., .F., .F.,
 ( 4, 4 ),
 ( 0.8794099815877536308, 0.8804107286285189904 ),
 .UNSPECIFIED. ) ;
#59000=CARTESIAN_POINT ( 'NONE',  ( -109.5228709571500474, -23.48783264082477018, -1.443836473390083253 ) ) ;
#59004=EDGE_LOOP ( 'NONE', ( #27504, #91887, #97942, #13371 ) ) ;
#59005=CARTESIAN_POINT ( 'NONE',  ( -74.52287095715007581, -24.34917612406836795, 0.1852690917426520756 ) ) ;
#59006=CARTESIAN_POINT ( 'NONE',  ( -69.52287095715003318, -24.66019654487199375, 8.947790411086119278 ) ) ;
#59007=CARTESIAN_POINT ( 'NONE',  ( -47.58190297339098151, -24.51314013834316086, 0.6176544820404172853 ) ) ;
#59008=CARTESIAN_POINT ( 'NONE',  ( -50.58953762381673158, -24.99156044556120193, 7.747789690856343725 ) ) ;
#59010=CARTESIAN_POINT ( 'NONE',  ( -99.62287095715005592, -23.48786465467241769, 11.44779295918254114 ) ) ;
#59012=CARTESIAN_POINT ( 'NONE',  ( -11.44242300287478820, -16.35863574123370512, 11.49999999999998934 ) ) ;
#59015=CARTESIAN_POINT ( 'NONE',  ( -0.08050249797735845037, -22.00783190155722480, 0.02034857451668616729 ) ) ;
#59016=VERTEX_POINT ( 'NONE', #80710 ) ;
#59017=CARTESIAN_POINT ( 'NONE',  ( -29.52287095715005805, -23.64127125214882597, -1.053577532865616950 ) ) ;
#59018=CARTESIAN_POINT ( 'NONE',  ( -63.52287095715006160, -24.64965694238575011, 8.947790433994201820 ) ) ;
#59023=CARTESIAN_POINT ( 'NONE',  ( -81.58510886217409563, -24.51314013834316796, 0.6176544820404249458 ) ) ;
#59024=CARTESIAN_POINT ( 'NONE',  ( -75.22287095715006444, -23.47593901973090169, -1.443836447538997536 ) ) ;
#59026=ORIENTED_EDGE ( 'NONE', *, *, #40204, .F. ) ;
#59027=CARTESIAN_POINT ( 'NONE',  ( -108.5228709571500616, -24.64965694238408034, 8.947790433994192938 ) ) ;
#59030=CARTESIAN_POINT ( 'NONE',  ( 8.375906630400100639, -18.44307005126401933, 11.49999999999998934 ) ) ;
#59031=CARTESIAN_POINT ( 'NONE',  ( -68.94158059132026040, -25.26655430154058735, 6.097253937284948577 ) ) ;
#59033=CARTESIAN_POINT ( 'NONE',  ( -109.6228709571500275, -24.50216790748098816, 0.6166512839513658140 ) ) ;
#59034=ORIENTED_EDGE ( 'NONE', *, *, #19892, .F. ) ;
#59035=CARTESIAN_POINT ( 'NONE',  ( -77.52287095715006160, -24.64965694238575011, 8.947790433994198267 ) ) ;
#59037=CARTESIAN_POINT ( 'NONE',  ( -14.83682921977595548, 13.52632505182701017, -1.500000000000002220 ) ) ;
#59038=CARTESIAN_POINT ( 'NONE',  ( -20.11743356864677423, -6.099313207006018089, 11.49999999999999645 ) ) ;
#59040=CARTESIAN_POINT ( 'NONE',  ( -70.53412792675530341, -24.92592662359561118, 8.075495903017998245 ) ) ;
#59041=CARTESIAN_POINT ( 'NONE',  ( -2.767897998228395551, 21.91458177938747909, 11.49999999999998934 ) ) ;
#59042=CARTESIAN_POINT ( 'NONE',  ( -60.45647255754339966, -25.29664575297535833, 6.028421396434780810 ) ) ;
#59043=EDGE_CURVE ( 'NONE', #56992, #83990, #73225, .T. ) ;
#59046=ORIENTED_EDGE ( 'NONE', *, *, #22669, .F. ) ;
#59047=CARTESIAN_POINT ( 'NONE',  ( -35.52287095715007581, -24.83620972994591014, 8.398175272781369216 ) ) ;
#59048=B_SPLINE_SURFACE_WITH_KNOTS ( 'NONE', 3, 1, ( 
 ( #72520, #10607 ),
 ( #3012, #63927 ),
 ( #25330, #86232 ),
 ( #32445, #9608 ),
 ( #80117, #41572 ),
 ( #47682, #24328 ),
 ( #79615, #78597 ),
 ( #54795, #71018 ),
 ( #55300, #86728 ),
 ( #70509, #47180 ),
 ( #85730, #78099 ) ),
 .UNSPECIFIED., .F., .F., .F.,
 ( 4, 1, 1, 1, 1, 1, 1, 1, 4 ),
 ( 2, 2 ),
 ( 0.000000000000000000, 0.1281355097972514123, 0.2541727119019812631, 0.3781116451390049149, 0.5017122630072827771, 0.6239863093684839823, 0.7470956136177411278, 0.8728746366500607090, 1.000000000000000000 ),
 ( 0.000000000000000000, 1.000000000000000000 ),
 .UNSPECIFIED. ) ;
#59049=CARTESIAN_POINT ( 'NONE',  ( -40.62287095715004170, -29.50249982740957577, 7.747779886224967605 ) ) ;
#59050=EDGE_CURVE ( 'NONE', #61038, #36448, #47887, .T. ) ;
#59051=ORIENTED_EDGE ( 'NONE', *, *, #54601, .T. ) ;
#59052=B_SPLINE_CURVE_WITH_KNOTS ( 'NONE', 3,
 ( #61194, #22091, #53074, #84002 ),
 .UNSPECIFIED., .F., .F.,
 ( 4, 4 ),
 ( 0.000000000000000000, 9.999999999996123101E-05 ),
 .UNSPECIFIED. ) ;
#59054=CARTESIAN_POINT ( 'NONE',  ( -83.55620429048339304, -24.65952944569304606, 1.056160979905699904 ) ) ;
#59057=CARTESIAN_POINT ( 'NONE',  ( -11.90445915685808131, 16.78794160864392992, -1.500000000000002220 ) ) ;
#59059=CARTESIAN_POINT ( 'NONE',  ( 20.98156868870745484, 4.911575462371418510, 11.49999999999999645 ) ) ;
#59060=ORIENTED_EDGE ( 'NONE', *, *, #54274, .T. ) ;
#59061=CARTESIAN_POINT ( 'NONE',  ( -91.62357778056286861, -24.65952944569304606, 1.056160979905701680 ) ) ;
#59064=CARTESIAN_POINT ( 'NONE',  ( 7.974090105135403839, 20.87195307945309963, 11.49999999999998934 ) ) ;
#59068=CARTESIAN_POINT ( 'NONE',  ( -124.6228709571500559, -23.73907113216991860, -1.053371485793223705 ) ) ;
#59071=CARTESIAN_POINT ( 'NONE',  ( -48.52287095715006160, -23.47596703998600631, 11.44779298504229104 ) ) ;
#59073=CARTESIAN_POINT ( 'NONE',  ( 17.92008016455634589, 10.74458801173053324, -1.500000000000002220 ) ) ;
#59077=VERTEX_POINT ( 'NONE', #80207 ) ;
#59078=ORIENTED_EDGE ( 'NONE', *, *, #31919, .F. ) ;
#59079=CARTESIAN_POINT ( 'NONE',  ( -51.29485095150216978, -25.26813275791670321, 4.047404401365850113 ) ) ;
#59080=CARTESIAN_POINT ( 'NONE',  ( 19.19679251752027227, 8.867671107084703408, -1.500000000000002220 ) ) ;
#59081=ORIENTED_EDGE ( 'NONE', *, *, #23641, .T. ) ;
#59082=CARTESIAN_POINT ( 'NONE',  ( -28.52287095715005805, -29.50248528299880846, 1.056150804693231082 ) ) ;
#59083=CARTESIAN_POINT ( 'NONE',  ( -98.58953762381672448, -23.48783264082478439, -1.443836473390061936 ) ) ;
#59084=CARTESIAN_POINT ( 'NONE',  ( -48.62287095715007013, -24.51387760970723662, 9.387446482453421837 ) ) ;
#59086=CARTESIAN_POINT ( 'NONE',  ( -80.62287095715005592, -29.50249982740957577, 7.747779886224967605 ) ) ;
#59087=CARTESIAN_POINT ( 'NONE',  ( -19.96617879207914825, 8.700599545123990808, -1.500000000000002220 ) ) ;
#59088=CARTESIAN_POINT ( 'NONE',  ( -80.40733119250255356, -25.04327900430719112, 7.562221853552162365 ) ) ;
#59089=CARTESIAN_POINT ( 'NONE',  ( -18.01732314745861530, 13.19606014829601826, 11.49999999999999645 ) ) ;
#59093=EDGE_CURVE ( 'NONE', #41820, #92347, #82912, .T. ) ;
#59094=CARTESIAN_POINT ( 'NONE',  ( -43.62287095715004881, -29.50247984919015209, -1.443849546365060466 ) ) ;
#59095=ORIENTED_EDGE ( 'NONE', *, *, #66917, .F. ) ;
#59096=VECTOR ( 'NONE', #61416, 1000.000000000000114 ) ;
#59097=ORIENTED_EDGE ( 'NONE', *, *, #51988, .T. ) ;
#59100=CARTESIAN_POINT ( 'NONE',  ( -100.7773612853930416, -25.13940139968743281, 7.065664229807540053 ) ) ;
#59101=B_SPLINE_CURVE_WITH_KNOTS ( 'NONE', 3,
 ( #89929, #35651, #99020, #44262 ),
 .UNSPECIFIED., .F., .F.,
 ( 4, 4 ),
 ( 0.000000000000000000, 9.999999999998206125E-05 ),
 .UNSPECIFIED. ) ;
#59102=CARTESIAN_POINT ( 'NONE',  ( -128.2228709571500644, -23.47593901973090524, -1.443836447538996204 ) ) ;
#59103=DIRECTION ( 'NONE',  ( -1.000000000000000000, -3.773278334444166432E-23, -8.201307841325785021E-29 ) ) ;
#59105=CARTESIAN_POINT ( 'NONE',  ( -87.52287095715006160, -24.64965694238575011, 8.947790433994196491 ) ) ;
#59107=ORIENTED_EDGE ( 'NONE', *, *, #64036, .F. ) ;
#59108=CARTESIAN_POINT ( 'NONE',  ( 19.38287969867323213, 0.6573286442255052986, 11.49999999999999645 ) ) ;
#59109=FACE_OUTER_BOUND ( 'NONE', #75742, .T. ) ;
#59111=DIRECTION ( 'NONE',  ( -0.000000000000000000, 2.173523156925979552E-06, -0.9999999999976378895 ) ) ;
#59113=FACE_OUTER_BOUND ( 'NONE', #70248, .T. ) ;
#59114=CARTESIAN_POINT ( 'NONE',  ( -130.5728709571500588, -23.47596703998600631, 11.44779298504227860 ) ) ;
#59116=CARTESIAN_POINT ( 'NONE',  ( 11.71876819965036809, 15.69520123712499249, -1.500000000000002220 ) ) ;
#59118=ORIENTED_EDGE ( 'NONE', *, *, #62372, .T. ) ;
#59119=AXIS2_PLACEMENT_3D ( 'NONE', #98523, #69468, #54258 ) ;
#59120=CARTESIAN_POINT ( 'NONE',  ( -14.38888013576714719, -16.06800976983558726, 11.49999999999998934 ) ) ;
#59121=CARTESIAN_POINT ( 'NONE',  ( -86.22287095715007865, -23.47596703998600631, 11.44779298504227860 ) ) ;
#59122=CARTESIAN_POINT ( 'NONE',  ( -108.9545715455115129, -29.50249205131699526, 4.170135655464190627 ) ) ;
#59123=CARTESIAN_POINT ( 'NONE',  ( -40.61244325972609914, -23.85016227208580730, -0.8807180028928393023 ) ) ;
#59125=LINE ( 'NONE', #90060, #98999 ) ;
#59126=CARTESIAN_POINT ( 'NONE',  ( 2.177599385301639323, -22.86303409451243596, -1.500000000000002220 ) ) ;
#59129=CARTESIAN_POINT ( 'NONE',  ( -49.49675345401667670, -25.29249258120279009, 4.255736650380444352 ) ) ;
#59130=CARTESIAN_POINT ( 'NONE',  ( -3.510519812331947875, -19.85243952969433323, 11.49999999999999645 ) ) ;
#59134=LINE ( 'NONE', #99651, #50481 ) ;
#59136=CARTESIAN_POINT ( 'NONE',  ( -10.37884456512175291, 16.95428827495986823, -1.500000000000002220 ) ) ;
#59137=CARTESIAN_POINT ( 'NONE',  ( -113.6235175983584753, -24.65952944569305316, 1.056160979905705011 ) ) ;
#59138=CARTESIAN_POINT ( 'NONE',  ( 17.76913753361954562, 8.601950719843506121, -1.500000000000002220 ) ) ;
#59142=CARTESIAN_POINT ( 'NONE',  ( -1.398219401198234957, 20.63772364298462847, 11.49999999999999645 ) ) ;
#59143=CARTESIAN_POINT ( 'NONE',  ( -39.26664729043937996, -25.31628629975991984, 5.049946001168161835 ) ) ;
#59144=VECTOR ( 'NONE', #70877, 1000.000000000000114 ) ;
#59146=CARTESIAN_POINT ( 'NONE',  ( 17.73637878876437668, -14.10177982315242318, 11.49999999999999645 ) ) ;
#59147=ORIENTED_EDGE ( 'NONE', *, *, #72127, .T. ) ;
#59150=DIRECTION ( 'NONE',  ( -3.773278334444167608E-23, 1.000000000000000000, 0.000000000000000000 ) ) ;
#59152=FACE_OUTER_BOUND ( 'NONE', #1073, .T. ) ;
#59154=VERTEX_POINT ( 'NONE', #25917 ) ;
#59156=CARTESIAN_POINT ( 'NONE',  ( 0.7049041324096299022, -22.85584899170066109, -1.500000000000002220 ) ) ;
#59157=CARTESIAN_POINT ( 'NONE',  ( -74.62287095715008434, -24.51283580621365132, 0.6167428607019774800 ) ) ;
#59158=CARTESIAN_POINT ( 'NONE',  ( 19.98928912078053699, -8.061568661392884749, -1.500000000000002220 ) ) ;
#59159=CARTESIAN_POINT ( 'NONE',  ( -92.52287095715006160, -29.50248528299804818, 1.056150453629040253 ) ) ;
#59160=CARTESIAN_POINT ( 'NONE',  ( -71.52287095715007581, -24.64898659630528854, 1.056161002820824368 ) ) ;
#59161=CARTESIAN_POINT ( 'NONE',  ( 17.82461400791848405, -13.82690402418615960, 11.49999999999999645 ) ) ;
#59163=CARTESIAN_POINT ( 'NONE',  ( -29.24566686208495625, -25.21112321003771584, 4.648180976733166325 ) ) ;
#59164=CARTESIAN_POINT ( 'NONE',  ( 10.07166557822571207, 19.55152498600455857, -1.500000000000002220 ) ) ;
#59165=FACE_OUTER_BOUND ( 'NONE', #22126, .T. ) ;
#59167=EDGE_CURVE ( 'NONE', #23809, #89711, #87784, .T. ) ;
#59169=CARTESIAN_POINT ( 'NONE',  ( -89.62287095715008434, -23.96177878511308990, 10.65340807706329862 ) ) ;
#59170=DIRECTION ( 'NONE',  ( -3.773278334444167608E-23, 1.000000000000000000, 0.000000000000000000 ) ) ;
#59171=ORIENTED_EDGE ( 'NONE', *, *, #49799, .F. ) ;
#59172=CARTESIAN_POINT ( 'NONE',  ( -108.5562042904834072, -23.47593901973091235, -1.443836447538999312 ) ) ;
#59174=ORIENTED_EDGE ( 'NONE', *, *, #22208, .T. ) ;
#59175=VERTEX_POINT ( 'NONE', #97428 ) ;
#59177=DIRECTION ( 'NONE',  ( -3.773278334453079030E-23, 0.9999999999976377785, 2.173523156925979128E-06 ) ) ;
#59179=B_SPLINE_CURVE_WITH_KNOTS ( 'NONE', 3,
 ( #94536, #72215, #56998, #8808, #54987, #85930 ),
 .UNSPECIFIED., .F., .F.,
 ( 4, 2, 4 ),
 ( 0.000000000000000000, 0.001380901958385382473, 0.002761803916770764946 ),
 .UNSPECIFIED. ) ;
#59180=CARTESIAN_POINT ( 'NONE',  ( -1.067026067711715154, -20.38227831319515460, -1.500000000000002220 ) ) ;
#59182=VERTEX_POINT ( 'NONE', #74100 ) ;
#59184=CARTESIAN_POINT ( 'NONE',  ( -60.92287095715005307, -23.47593901973090169, -1.443836447538997536 ) ) ;
#59185=EDGE_CURVE ( 'NONE', #67908, #13108, #91358, .T. ) ;
#59186=FACE_OUTER_BOUND ( 'NONE', #43070, .T. ) ;
#59187=CARTESIAN_POINT ( 'NONE',  ( -70.70237668956666255, -25.03149840991684982, 7.522646895911706544 ) ) ;
#59191=EDGE_CURVE ( 'NONE', #25617, #27620, #5465, .T. ) ;
#59193=ORIENTED_EDGE ( 'NONE', *, *, #98965, .T. ) ;
#59194=EDGE_CURVE ( 'NONE', #40854, #6116, #27219, .T. ) ;
#59195=CARTESIAN_POINT ( 'NONE',  ( -3.686900873480770002, -20.48319827837541141, 11.49999999999998934 ) ) ;
#59196=EDGE_LOOP ( 'NONE', ( #38096, #43259, #398, #45076 ) ) ;
#59197=FACE_OUTER_BOUND ( 'NONE', #5255, .T. ) ;
#59198=ORIENTED_EDGE ( 'NONE', *, *, #7999, .T. ) ;
#59200=DIRECTION ( 'NONE',  ( -1.000000000000000000, -3.773278334444166432E-23, -8.201307841325785021E-29 ) ) ;
#59201=ORIENTED_EDGE ( 'NONE', *, *, #27889, .T. ) ;
#59203=CARTESIAN_POINT ( 'NONE',  ( -25.53098197642538736, -29.50249373072461623, 4.942801737957442931 ) ) ;
#59206=CARTESIAN_POINT ( 'NONE',  ( -43.65489518069405506, -23.73791477778911130, 11.05961554403171121 ) ) ;
#59207=CARTESIAN_POINT ( 'NONE',  ( -9.153499762860807465, 20.15527781828815534, 11.49999999999999645 ) ) ;
#59208=EDGE_LOOP ( 'NONE', ( #99348, #15100, #16690, #21994 ) ) ;
#59209=CARTESIAN_POINT ( 'NONE',  ( -72.62287095715007013, -23.96127896941632685, -0.6493128931037881468 ) ) ;
#59210=CARTESIAN_POINT ( 'NONE',  ( -7.157701736792966507, -21.45640540170154509, 11.49999999999998934 ) ) ;
#59211=CARTESIAN_POINT ( 'NONE',  ( -115.5902947577247346, -24.40133493613050675, 9.663955038902797057 ) ) ;
#59212=VERTEX_POINT ( 'NONE', #34539 ) ;
#59215=AXIS2_PLACEMENT_3D ( 'NONE', #33313, #79494, #86605 ) ;
#59216=CARTESIAN_POINT ( 'NONE',  ( -78.62287095715005592, -23.47596703998600631, 11.44779298504227860 ) ) ;
#59217=ORIENTED_EDGE ( 'NONE', *, *, #98144, .F. ) ;
#59218=CARTESIAN_POINT ( 'NONE',  ( -89.52287095715006160, -24.35013146730203815, 9.818937971375097717 ) ) ;
#59219=CARTESIAN_POINT ( 'NONE',  ( -17.34812393562427246, -13.96779696820907191, -1.500000000000002220 ) ) ;
#59220=CARTESIAN_POINT ( 'NONE',  ( -121.5228709571500616, -29.50250243563736774, 8.947779886222134493 ) ) ;
#59222=ORIENTED_EDGE ( 'NONE', *, *, #70788, .F. ) ;
#59224=CARTESIAN_POINT ( 'NONE',  ( -80.59883725225060402, -25.03321342637004321, 7.561462816580968749 ) ) ;
#59227=CARTESIAN_POINT ( 'NONE',  ( -108.6228709571501128, -24.34917612406838217, 0.1852690917426704775 ) ) ;
#59228=CARTESIAN_POINT ( 'NONE',  ( -65.62287095715005592, -29.50248528299804818, 1.056150453629036701 ) ) ;
#59229=CARTESIAN_POINT ( 'NONE',  ( 5.544562197198338538, -18.70016399976332977, 11.49999999999998934 ) ) ;
#59230=CARTESIAN_POINT ( 'NONE',  ( 19.78805588120126302, 8.271231038663975355, 11.49999999999998934 ) ) ;
#59233=CARTESIAN_POINT ( 'NONE',  ( -76.52287095715007581, -23.48786465467241769, 11.44779295918254469 ) ) ;
#59234=EDGE_CURVE ( 'NONE', #52326, #4648, #78052, .T. ) ;
#59235=CARTESIAN_POINT ( 'NONE',  ( -10.82450569625279613, 20.10975305113172951, -1.500000000000002220 ) ) ;
#59236=EDGE_CURVE ( 'NONE', #96161, #78575, #51484, .T. ) ;
#59239=FACE_OUTER_BOUND ( 'NONE', #63928, .T. ) ;
#59240=CARTESIAN_POINT ( 'NONE',  ( 4.608267332293128682, -19.41724391825443874, 11.49999999999999645 ) ) ;
#59241=DIRECTION ( 'NONE',  ( -3.773278334444166432E-23, 1.000000000000000000, 0.000000000000000000 ) ) ;
#59242=B_SPLINE_CURVE_WITH_KNOTS ( 'NONE', 3,
 ( #31060, #71531, #25841, #33959 ),
 .UNSPECIFIED., .F., .F.,
 ( 4, 4 ),
 ( 0.000000000000000000, 9.999999999998897304E-05 ),
 .UNSPECIFIED. ) ;
#59243=CARTESIAN_POINT ( 'NONE',  ( -39.66519142177316581, -23.48786465467240703, 11.44779295918255002 ) ) ;
#59244=B_SPLINE_CURVE_WITH_KNOTS ( 'NONE', 3,
 ( #45216, #5642, #29471, #76142, #84763, #15250 ),
 .UNSPECIFIED., .F., .F.,
 ( 4, 2, 4 ),
 ( 0.000000000000000000, 0.001380901958385387894, 0.002761803916770775788 ),
 .UNSPECIFIED. ) ;
#59245=CARTESIAN_POINT ( 'NONE',  ( -101.6228709571500559, -23.94994826722515668, -0.6494450866351716423 ) ) ;
#59247=CARTESIAN_POINT ( 'NONE',  ( -25.53615934357976869, -24.91998285861100371, 4.571435626871006797 ) ) ;
#59249=CARTESIAN_POINT ( 'NONE',  ( 3.708801897538985148, -21.39311272803122321, -1.500000000000002220 ) ) ;
#59250=CARTESIAN_POINT ( 'NONE',  ( -77.52287095715006160, -24.66019654487200086, 8.947790411086113949 ) ) ;
#59251=CARTESIAN_POINT ( 'NONE',  ( 18.00893756148942870, 7.586210683597776949, -1.500000000000002220 ) ) ;
#59252=CARTESIAN_POINT ( 'NONE',  ( -99.31324271614009547, -25.24395871390426294, 6.321204267077806804 ) ) ;
#59253=VERTEX_POINT ( 'NONE', #47886 ) ;
#59255=VECTOR ( 'NONE', #60156, 1000.000000000000114 ) ;
#59257=CARTESIAN_POINT ( 'NONE',  ( -110.6228709571500701, -24.92579138211019441, 1.929029949965667123 ) ) ;
#59258=CARTESIAN_POINT ( 'NONE',  ( -10.82153711268468932, 17.32902648900640230, 11.49999999999999645 ) ) ;
#59259=CARTESIAN_POINT ( 'NONE',  ( -49.28534510465767937, -25.26380556882021722, 6.011612785043525697 ) ) ;
#59261=EDGE_LOOP ( 'NONE', ( #26242, #89846, #23999, #39594 ) ) ;
#59262=CARTESIAN_POINT ( 'NONE',  ( -51.62287095715005592, -23.47593901973091235, -1.443836447539009749 ) ) ;
#59266=VERTEX_POINT ( 'NONE', #41270 ) ;
#59268=CARTESIAN_POINT ( 'NONE',  ( -22.84742429131147645, -2.885717679200183738, 11.49999999999999645 ) ) ;
#59269=CARTESIAN_POINT ( 'NONE',  ( -22.16177213047534877, -5.259615592301647879, 11.49999999999998934 ) ) ;
#59271=DIRECTION ( 'NONE',  ( 0.000000000000000000, 2.173523156925980399E-06, -0.9999999999976378895 ) ) ;
#59272=CARTESIAN_POINT ( 'NONE',  ( -108.9545715455114987, -25.28708312187852414, 4.170144817753115518 ) ) ;
#59273=CARTESIAN_POINT ( 'NONE',  ( -71.62287095715005592, -29.50250786944525672, 11.44777988621623699 ) ) ;
#59274=CARTESIAN_POINT ( 'NONE',  ( -99.25999413675920380, -25.30157743809076720, 5.189783768456954327 ) ) ;
#59275=CARTESIAN_POINT ( 'NONE',  ( -14.06357901826416068, -16.81340526219955933, -1.500000000000002220 ) ) ;
#59279=CARTESIAN_POINT ( 'NONE',  ( -71.27032225721183067, -25.30598519668817303, 4.985731859564575430 ) ) ;
#59280=CARTESIAN_POINT ( 'NONE',  ( -58.63776290787987477, -24.15543982623907127, -0.2315651400026660645 ) ) ;
#59282=VECTOR ( 'NONE', #6655, 1000.000000000000114 ) ;
#59283=EDGE_CURVE ( 'NONE', #69140, #13751, #99783, .T. ) ;
#59284=CARTESIAN_POINT ( 'NONE',  ( 20.25987197511681259, 2.754759976156288204, 11.49999999999998934 ) ) ;
#59287=EDGE_LOOP ( 'NONE', ( #46830, #38064, #61158, #30957 ) ) ;
#59289=ORIENTED_EDGE ( 'NONE', *, *, #71467, .F. ) ;
#59290=CARTESIAN_POINT ( 'NONE',  ( -16.13607370526515794, 16.44073208242836159, -1.500000000000002220 ) ) ;
#59291=CARTESIAN_POINT ( 'NONE',  ( -63.62287095715004881, -24.66019654487199020, 8.947790411086131712 ) ) ;
#59292=CARTESIAN_POINT ( 'NONE',  ( -20.17641613807547785, 1.360797614858565874, -1.500000000000002220 ) ) ;
#59293=AXIS2_PLACEMENT_3D ( 'NONE', #87175, #56249, #49134 ) ;
#59294=EDGE_CURVE ( 'NONE', #17515, #56546, #28455, .T. ) ;
#59296=CARTESIAN_POINT ( 'NONE',  ( -98.62287095715008434, -24.50321055353806443, 9.387540953477520489 ) ) ;
#59299=ADVANCED_FACE ( 'NONE', ( #32647 ), #64637, .F. ) ;
#59300=CARTESIAN_POINT ( 'NONE',  ( -101.5228709571501042, -24.35013146730203104, 9.818937971375097717 ) ) ;
#59301=CARTESIAN_POINT ( 'NONE',  ( -99.58504437842513823, -24.66019654487200086, 8.947790411086115725 ) ) ;
#59302=CARTESIAN_POINT ( 'NONE',  ( 9.988417798295188277, 18.97302403871600518, 11.49999999999999645 ) ) ;
#59304=PLANE ( 'NONE',  #37089 ) ;
#59305=ADVANCED_FACE ( 'NONE', ( #50886 ), #57511, .T. ) ;
#59306=VERTEX_POINT ( 'NONE', #67118 ) ;
#59307=CARTESIAN_POINT ( 'NONE',  ( 21.95989154999629278, -3.605859658025859282, -1.500000000000002220 ) ) ;
#59309=CARTESIAN_POINT ( 'NONE',  ( 12.98984941077313415, -16.12360325096057423, -1.500000000000002220 ) ) ;
#59313=DIRECTION ( 'NONE',  ( 0.000000000000000000, 0.9999999999976377785, 2.173523156925979975E-06 ) ) ;
#59315=CARTESIAN_POINT ( 'NONE',  ( 19.98859412959824411, 6.261702723725245612, -1.500000000000002220 ) ) ;
#59317=CARTESIAN_POINT ( 'NONE',  ( -8.322136096487577461, -20.27582920440508829, 11.49999999999999645 ) ) ;
#59318=CARTESIAN_POINT ( 'NONE',  ( -37.51295737854163548, -23.73791477778911130, 11.05961554403171299 ) ) ;
#59319=CARTESIAN_POINT ( 'NONE',  ( -0.06565682164858396841, -22.51586213336150166, 11.49999999999998934 ) ) ;
#59320=CARTESIAN_POINT ( 'NONE',  ( -7.049398010371669798, 19.71092172866906012, 11.49999999999998934 ) ) ;
#59322=CARTESIAN_POINT ( 'NONE',  ( -91.58953762381672448, -23.48783264082478794, -1.443836473390063713 ) ) ;
#59324=ORIENTED_EDGE ( 'NONE', *, *, #78333, .T. ) ;
#59326=ORIENTED_EDGE ( 'NONE', *, *, #24091, .F. ) ;
#59327=CARTESIAN_POINT ( 'NONE',  ( -128.6228709571500417, -24.51387760970725083, 9.387446482453409402 ) ) ;
#59328=CARTESIAN_POINT ( 'NONE',  ( -16.68621059303058018, 13.52761613308161870, -1.500000000000002220 ) ) ;
#59329=CARTESIAN_POINT ( 'NONE',  ( -105.5228709571500758, -23.47596703998600631, 11.44779298504228038 ) ) ;
#59330=VERTEX_POINT ( 'NONE', #59489 ) ;
#59331=CARTESIAN_POINT ( 'NONE',  ( -16.97324839047195866, 12.58421825509937442, -1.500000000000002220 ) ) ;
#59333=CARTESIAN_POINT ( 'NONE',  ( -119.6228709571500559, -29.50250243563736774, 8.947779886222134493 ) ) ;
#59337=CARTESIAN_POINT ( 'NONE',  ( -7.692412698405892257, 20.70400481474656118, -1.500000000000002220 ) ) ;
#59338=CARTESIAN_POINT ( 'NONE',  ( -81.58232365645901041, -24.66019654487198665, 8.947790411086131712 ) ) ;
#59339=CARTESIAN_POINT ( 'NONE',  ( -51.92928322226379123, -25.31633332227261235, 6.080069373430273316 ) ) ;
#59340=DIRECTION ( 'NONE',  ( -3.773278334453079618E-23, 0.9999999999976377785, 2.173523156925979975E-06 ) ) ;
#59344=CARTESIAN_POINT ( 'NONE',  ( -14.39514105012195344, 13.04300321504834947, -1.500000000000002220 ) ) ;
#59345=CARTESIAN_POINT ( 'NONE',  ( 4.555389213293416617, -20.86945110937667280, 11.49999999999998934 ) ) ;
#59347=CARTESIAN_POINT ( 'NONE',  ( -50.91713042577481474, -25.30060005375479903, 6.009289253917323492 ) ) ;
#59348=ADVANCED_FACE ( 'NONE', ( #43274 ), #20907, .T. ) ;
#59349=CARTESIAN_POINT ( 'NONE',  ( -64.60984581131128834, -23.48786465467241058, 11.44779295918254824 ) ) ;
#59350=CARTESIAN_POINT ( 'NONE',  ( -126.6228709571500843, -24.66019654487200441, 8.947790411086119278 ) ) ;
#59351=CARTESIAN_POINT ( 'NONE',  ( 8.023449251107201974, -21.19570997880782670, -1.500000000000002220 ) ) ;
#59355=B_SPLINE_CURVE_WITH_KNOTS ( 'NONE', 3,
 ( #52687, #60811, #13109, #22213, #84126, #35960 ),
 .UNSPECIFIED., .F., .F.,
 ( 4, 2, 4 ),
 ( 0.000000000000000000, 0.001380764517853256840, 0.002761529035706513681 ),
 .UNSPECIFIED. ) ;
#59356=CARTESIAN_POINT ( 'NONE',  ( -87.52287095715006160, -23.48786465467241058, 11.44779295918254292 ) ) ;
#59357=CARTESIAN_POINT ( 'NONE',  ( -69.92287095715005307, -23.47593901973090169, -1.443836447538997536 ) ) ;
#59358=CARTESIAN_POINT ( 'NONE',  ( -11.05534852661189937, -16.44151763790470966, 11.49999999999999645 ) ) ;
#59360=AXIS2_PLACEMENT_3D ( 'NONE', #66694, #29089, #60063 ) ;
#59362=ORIENTED_EDGE ( 'NONE', *, *, #19667, .F. ) ;
#59363=B_SPLINE_CURVE_WITH_KNOTS ( 'NONE', 3,
 ( #51856, #67095, #22367, #75661 ),
 .UNSPECIFIED., .F., .F.,
 ( 4, 4 ),
 ( 0.000000000000000000, 9.999999999998206125E-05 ),
 .UNSPECIFIED. ) ;
#59365=CARTESIAN_POINT ( 'NONE',  ( -128.6228709571500417, -24.64965695001469115, 8.947790433994173398 ) ) ;
#59366=CARTESIAN_POINT ( 'NONE',  ( -70.52287095715007581, -25.00182538069145366, 7.747789668545101094 ) ) ;
#59367=CARTESIAN_POINT ( 'NONE',  ( -100.6597906528727577, -25.12268562698065111, 7.087518430423694227 ) ) ;
#59368=CARTESIAN_POINT ( 'NONE',  ( -12.93760099376155104, 17.33828479246177423, -1.500000000000002220 ) ) ;
#59369=CARTESIAN_POINT ( 'NONE',  ( -49.10668015502195516, -25.27518120313465033, 3.950017688817143213 ) ) ;
#59371=CARTESIAN_POINT ( 'NONE',  ( -5.798782886354239885, 18.49141925852020663, -1.500000000000002220 ) ) ;
#59373=CARTESIAN_POINT ( 'NONE',  ( -82.62287095714999907, -23.96177878511307568, 10.65340807706330395 ) ) ;
#59374=CARTESIAN_POINT ( 'NONE',  ( -12.28770250403618114, -15.54288071925545722, 11.49999999999998934 ) ) ;
#59375=VERTEX_POINT ( 'NONE', #74215 ) ;
#59376=CARTESIAN_POINT ( 'NONE',  ( 16.63042848490962555, -11.55671354112608817, 11.49999999999999645 ) ) ;
#59377=CARTESIAN_POINT ( 'NONE',  ( -71.70841769935766763, -29.50249644799903592, 6.192972193920951440 ) ) ;
#59378=B_SPLINE_CURVE_WITH_KNOTS ( 'NONE', 3,
 ( #81973, #49173, #1488, #10088 ),
 .UNSPECIFIED., .F., .F.,
 ( 4, 4 ),
 ( 0.8303788777084928352, 0.8393853089806082579 ),
 .UNSPECIFIED. ) ;
#59380=CARTESIAN_POINT ( 'NONE',  ( -111.6228709571500559, -23.48783264082479505, -1.443836473390060604 ) ) ;
#59384=CARTESIAN_POINT ( 'NONE',  ( -99.62287095715005592, -23.48786465467241769, 11.44779295918254114 ) ) ;
#59386=CARTESIAN_POINT ( 'NONE',  ( -31.52287095715006160, -24.64965694238574656, 8.947790433994207149 ) ) ;
#59387=CARTESIAN_POINT ( 'NONE',  ( -19.96166555454951208, -2.086822695551191043, 11.49999999999998934 ) ) ;
#59389=ORIENTED_EDGE ( 'NONE', *, *, #21910, .F. ) ;
#59391=CARTESIAN_POINT ( 'NONE',  ( -49.62307173802614102, -25.31297133582045333, 4.349864010778793144 ) ) ;
#59396=CARTESIAN_POINT ( 'NONE',  ( 14.42577177192597482, -17.14957960503723911, 11.49999999999999645 ) ) ;
#59397=DIRECTION ( 'NONE',  ( 0.000000000000000000, 0.9999999999976377785, 2.173523156925979128E-06 ) ) ;
#59399=CARTESIAN_POINT ( 'NONE',  ( 2.178911383790714584, -20.24183328246387958, -1.500000000000002220 ) ) ;
#59400=VERTEX_POINT ( 'NONE', #82810 ) ;
#59401=EDGE_CURVE ( 'NONE', #73893, #61226, #80831, .T. ) ;
#59402=CARTESIAN_POINT ( 'NONE',  ( 12.10309942457327992, -19.51426552955538085, -1.500000000000002220 ) ) ;
#59403=CARTESIAN_POINT ( 'NONE',  ( -53.52287095715006870, -23.48786465467241058, 11.44779295918255002 ) ) ;
#59405=CARTESIAN_POINT ( 'NONE',  ( -49.17793306806408538, -25.29053177449054957, 4.390131398629820048 ) ) ;
#59408=CARTESIAN_POINT ( 'NONE',  ( -95.62287095715007013, -23.48786465467241769, 11.44779295918254114 ) ) ;
#59409=CARTESIAN_POINT ( 'NONE',  ( 20.41123533131232648, 5.719371238976541427, 11.49999999999999645 ) ) ;
#59410=ORIENTED_EDGE ( 'NONE', *, *, #44637, .F. ) ;
#59413=CARTESIAN_POINT ( 'NONE',  ( -7.471142097702432316, -20.87072022463130239, 11.49999999999998934 ) ) ;
#59415=CARTESIAN_POINT ( 'NONE',  ( -10.57813111170615983, 17.65445453266677234, -1.500000000000002220 ) ) ;
#59416=VECTOR ( 'NONE', #92910, 1000.000000000000114 ) ;
#59417=ORIENTED_EDGE ( 'NONE', *, *, #72123, .F. ) ;
#59420=CARTESIAN_POINT ( 'NONE',  ( -40.43756433397305017, -25.12049752546737835, 2.832404795212222659 ) ) ;
#59421=ORIENTED_EDGE ( 'NONE', *, *, #92375, .T. ) ;
#59422=VECTOR ( 'NONE', #75758, 1000.000000000000114 ) ;
#59423=VERTEX_POINT ( 'NONE', #89935 ) ;
#59426=FACE_OUTER_BOUND ( 'NONE', #39814, .T. ) ;
#59427=B_SPLINE_CURVE_WITH_KNOTS ( 'NONE', 3,
 ( #85002, #7376, #38330, #54080, #15486, #77379 ),
 .UNSPECIFIED., .F., .F.,
 ( 4, 2, 4 ),
 ( 6.391158118956848875E-06, 0.001387004593080773136, 0.002767618028042589419 ),
 .UNSPECIFIED. ) ;
#59428=CARTESIAN_POINT ( 'NONE',  ( -28.67154396960757268, -23.33526543178592050, 11.44779300624183982 ) ) ;
#59429=CARTESIAN_POINT ( 'NONE',  ( -33.52287095715006160, -23.47593901973090169, -1.443836447538997314 ) ) ;
#59430=CARTESIAN_POINT ( 'NONE',  ( 14.61947915221463923, 14.71393552341326760, -1.500000000000002220 ) ) ;
#59431=ADVANCED_FACE ( 'NONE', ( #3228 ), #34162, .T. ) ;
#59432=CARTESIAN_POINT ( 'NONE',  ( -9.282276271697774916, -19.63344595494797673, 11.49999999999999645 ) ) ;
#59433=VERTEX_POINT ( 'NONE', #27041 ) ;
#59434=CARTESIAN_POINT ( 'NONE',  ( -40.41683116089613748, -25.31583771263539973, 5.082404370641117275 ) ) ;
#59435=CARTESIAN_POINT ( 'NONE',  ( -37.52287095715006870, -24.66019654487199375, 8.947790411086122830 ) ) ;
#59436=CARTESIAN_POINT ( 'NONE',  ( -115.5505219823595979, -24.92564183028979130, 1.928384488918252870 ) ) ;
#59437=CARTESIAN_POINT ( 'NONE',  ( -22.41777205227948855, 0.6913007675000180097, 11.49999999999998934 ) ) ;
#59438=VECTOR ( 'NONE', #35916, 1000.000000000000114 ) ;
#59439=CARTESIAN_POINT ( 'NONE',  ( -51.28074245548943111, -25.31296633745817815, 4.131999440082223529 ) ) ;
#59440=CARTESIAN_POINT ( 'NONE',  ( -124.5228709571500190, -24.66019654487200441, 8.947790411086112172 ) ) ;
#59441=ORIENTED_EDGE ( 'NONE', *, *, #2502, .F. ) ;
#59442=CARTESIAN_POINT ( 'NONE',  ( -75.52287095715009002, -24.62226745350438506, 0.9660975649728140713 ) ) ;
#59445=ORIENTED_EDGE ( 'NONE', *, *, #83495, .F. ) ;
#59446=CARTESIAN_POINT ( 'NONE',  ( -100.0593466484916831, -25.31258597278857536, 5.273631863065838310 ) ) ;
#59448=CARTESIAN_POINT ( 'NONE',  ( -20.90244970016518877, -3.954922567530639199, -1.500000000000002220 ) ) ;
#59449=ORIENTED_EDGE ( 'NONE', *, *, #84335, .T. ) ;
#59451=CARTESIAN_POINT ( 'NONE',  ( 17.34737195785526609, 13.27887811287985187, 11.49999999999998934 ) ) ;
#59452=CARTESIAN_POINT ( 'NONE',  ( -55.58953762381671737, -23.47596703998600276, 11.44779298504227505 ) ) ;
#59453=CARTESIAN_POINT ( 'NONE',  ( 2.290073164716609710, 22.57640404599860418, 11.49999999999998934 ) ) ;
#59454=CARTESIAN_POINT ( 'NONE',  ( -40.84535658588885099, -25.28892436072735705, 3.358264504957044760 ) ) ;
#59455=CARTESIAN_POINT ( 'NONE',  ( -28.92287095928432095, -23.34274621196139421, 11.44779298504227860 ) ) ;
#59456=CARTESIAN_POINT ( 'NONE',  ( -21.55542221127511482, -4.010009934288176758, -1.500000000000002220 ) ) ;
#59457=CARTESIAN_POINT ( 'NONE',  ( -87.51421903235882382, -23.96119346886881729, -0.6495511937831870419 ) ) ;
#59459=CARTESIAN_POINT ( 'NONE',  ( -37.62287095715007013, -23.47596703998600276, 11.44779298504227505 ) ) ;
#59461=VECTOR ( 'NONE', #69283, 1000.000000000000114 ) ;
#59462=ORIENTED_EDGE ( 'NONE', *, *, #71191, .T. ) ;
#59463=CARTESIAN_POINT ( 'NONE',  ( -116.6228709571500701, -23.72747288104470087, -1.053458166803224350 ) ) ;
#59464=B_SPLINE_CURVE_WITH_KNOTS ( 'NONE', 3,
 ( #53226, #84658, #69934, #84154 ),
 .UNSPECIFIED., .F., .F.,
 ( 4, 4 ),
 ( 0.000000000000000000, 1.000000000000000000 ),
 .UNSPECIFIED. ) ;
#59465=CARTESIAN_POINT ( 'NONE',  ( -128.5228709571500474, -23.48783264083417066, -1.443836473375472274 ) ) ;
#59467=CARTESIAN_POINT ( 'NONE',  ( -0.1256113942619183077, -21.42386179076044073, -0.9709657327914291702 ) ) ;
#59468=CARTESIAN_POINT ( 'NONE',  ( -8.014198274750887308, -19.69740135394370384, -1.500000000000002220 ) ) ;
#59469=CARTESIAN_POINT ( 'NONE',  ( -112.5150172138885694, -24.51314013834317151, 0.6176544820404297198 ) ) ;
#59471=CARTESIAN_POINT ( 'NONE',  ( -114.5228709571500332, -24.34917612407039655, 0.1852690917479089538 ) ) ;
#59472=CARTESIAN_POINT ( 'NONE',  ( -70.52287095715009002, -24.51163499207179797, 0.6490370598555543769 ) ) ;
#59474=B_SPLINE_SURFACE_WITH_KNOTS ( 'NONE', 3, 1, ( 
 ( #43483, #42497 ),
 ( #3929, #88657 ),
 ( #90640, #12019 ),
 ( #67317, #80533 ),
 ( #4422, #73432 ),
 ( #35372, #59709 ),
 ( #96758, #11027 ),
 ( #66833, #27257 ),
 ( #58211, #34367 ),
 ( #20624, #13006 ),
 ( #41997, #65347 ),
 ( #72934, #97754 ),
 ( #12516, #51591 ),
 ( #81545, #43972 ),
 ( #96265, #66335 ),
 ( #82036, #28747 ),
 ( #82526, #89648 ),
 ( #98242, #20130 ),
 ( #74904, #3434 ) ),
 .UNSPECIFIED., .F., .F., .F.,
 ( 4, 1, 1, 1, 1, 1, 1, 1, 1, 1, 1, 1, 1, 1, 1, 1, 4 ),
 ( 2, 2 ),
 ( 0.000000000000000000, 0.07059928943359371212, 0.1379009210036218069, 0.2031961978097392985, 0.2667897246502602959, 0.3291063872214292640, 0.3906535452348646187, 0.4526530569344794919, 0.5157480403003763536, 0.5779263408004525759, 0.6389300116184458700, 0.6983507176418246587, 0.7572960374442720966, 0.8163937673501532322, 0.8762669096141292302, 0.9368171089060849388, 1.000000000000000000 ),
 ( 0.000000000000000000, 1.000000000000000000 ),
 .UNSPECIFIED. ) ;
#59475=CARTESIAN_POINT ( 'NONE',  ( -117.5198278380623123, -23.96169478059714564, 10.65365249895717170 ) ) ;
#59477=CARTESIAN_POINT ( 'NONE',  ( -16.94305004876727239, 9.801747318927828800, 11.49999999999999645 ) ) ;
#59478=DIRECTION ( 'NONE',  ( 0.000000000000000000, -2.173523156925979552E-06, 0.9999999999976378895 ) ) ;
#59479=CARTESIAN_POINT ( 'NONE',  ( -100.6228709571500985, -24.14406661707771207, 10.28769366152061160 ) ) ;
#59480=VERTEX_POINT ( 'NONE', #73712 ) ;
#59481=CARTESIAN_POINT ( 'NONE',  ( -117.5228709571500616, -24.50321055353804311, 9.387540953477508054 ) ) ;
#59482=CARTESIAN_POINT ( 'NONE',  ( -40.58953762381672448, -23.47596703998600276, 11.44779298504227505 ) ) ;
#59484=CARTESIAN_POINT ( 'NONE',  ( -116.5228709571499905, -23.48783264083416711, -1.443836473375476270 ) ) ;
#59485=CARTESIAN_POINT ( 'NONE',  ( -50.40445135320379677, -25.12298712672050982, 7.101635559041870494 ) ) ;
#59486=CARTESIAN_POINT ( 'NONE',  ( -19.67082186522023690, -1.387426831159568108, 11.49999999999998934 ) ) ;
#59488=PLANE ( 'NONE',  #8407 ) ;
#59489=CARTESIAN_POINT ( 'NONE',  ( -112.5228709571500616, -24.64898659630529210, 1.056161002820831474 ) ) ;
#59490=VECTOR ( 'NONE', #95221, 1000.000000000000114 ) ;
#59491=EDGE_CURVE ( 'NONE', #54673, #53154, #97477, .T. ) ;
#59493=ORIENTED_EDGE ( 'NONE', *, *, #37125, .F. ) ;
#59495=CARTESIAN_POINT ( 'NONE',  ( -45.62287095715004170, -23.85229601348996198, 10.88205029486207742 ) ) ;
#59496=CARTESIAN_POINT ( 'NONE',  ( -47.58717649367020641, -24.34968618360933590, 0.1864209137778879144 ) ) ;
#59497=CARTESIAN_POINT ( 'NONE',  ( -50.55620429048339304, -24.99156044556202261, 7.747789690856172307 ) ) ;
#59498=FACE_OUTER_BOUND ( 'NONE', #86616, .T. ) ;
#59503=CARTESIAN_POINT ( 'NONE',  ( -112.5228709571500332, -23.94994826722564696, -0.6494450866342713624 ) ) ;
#59504=CARTESIAN_POINT ( 'NONE',  ( -18.20579941527595480, -8.200869797747142087, -1.500000000000002220 ) ) ;
#59505=B_SPLINE_CURVE_WITH_KNOTS ( 'NONE', 3,
 ( #18907, #18416, #26537, #80315 ),
 .UNSPECIFIED., .F., .F.,
 ( 4, 4 ),
 ( 0.000000000000000000, 9.999999999998897304E-05 ),
 .UNSPECIFIED. ) ;
#59507=CARTESIAN_POINT ( 'NONE',  ( -0.1426030150137701236, -21.20389190742571373, -1.497999999999532594 ) ) ;
#59512=EDGE_CURVE ( 'NONE', #21092, #40713, #53381, .T. ) ;
#59513=CARTESIAN_POINT ( 'NONE',  ( -119.5532611137347914, -24.51314013834316086, 0.6176544820404233915 ) ) ;
#59515=DIRECTION ( 'NONE',  ( 0.000000000000000000, -0.9999999999976377785, -2.173523156925979975E-06 ) ) ;
#59516=CARTESIAN_POINT ( 'NONE',  ( -126.3652925398622529, -25.21789590547953352, 6.462002543204359739 ) ) ;
#59517=CARTESIAN_POINT ( 'NONE',  ( -39.62372002940962545, -24.65952944569304250, 1.056160979905697017 ) ) ;
#59518=CARTESIAN_POINT ( 'NONE',  ( -72.62287095715009855, -23.95044443724992433, 10.65354141964649948 ) ) ;
#59519=CARTESIAN_POINT ( 'NONE',  ( -51.53844848903055009, -25.31574372701962616, 4.526031553223371695 ) ) ;
#59520=ORIENTED_EDGE ( 'NONE', *, *, #4977, .T. ) ;
#59522=CARTESIAN_POINT ( 'NONE',  ( -127.5552457623996787, -24.51314013834318217, 0.6176544820404269442 ) ) ;
#59523=EDGE_LOOP ( 'NONE', ( #80536, #69899, #81667, #94321 ) ) ;
#59524=CARTESIAN_POINT ( 'NONE',  ( 20.24638344296597836, 0.1212440198127159030, 11.49999999999998934 ) ) ;
#59527=DIRECTION ( 'NONE',  ( -3.773278334453079030E-23, 0.9999999999976377785, 2.173523156925979128E-06 ) ) ;
#59529=DIRECTION ( 'NONE',  ( 0.000000000000000000, -0.9999999999976377785, -2.173523156925979975E-06 ) ) ;
#59531=CARTESIAN_POINT ( 'NONE',  ( -80.26322933785027658, -25.30551634214781132, 4.507558500180725680 ) ) ;
#59532=LINE ( 'NONE', #81365, #14636 ) ;
#59533=CARTESIAN_POINT ( 'NONE',  ( 14.85562765054232059, -13.46834898924134372, -1.500000000000002220 ) ) ;
#59534=CARTESIAN_POINT ( 'NONE',  ( -5.295558097854481616, 20.35707381486366785, 11.49999999999999645 ) ) ;
#59536=CARTESIAN_POINT ( 'NONE',  ( -27.68651082257923690, -24.80976250947271211, 7.605672514646787619 ) ) ;
#59537=CARTESIAN_POINT ( 'NONE',  ( -70.50070265878940745, -24.40133493613049964, 9.663955038902802386 ) ) ;
#59538=CARTESIAN_POINT ( 'NONE',  ( -16.08457400211760913, 15.13120210334024662, 11.49999999999998934 ) ) ;
#59540=CARTESIAN_POINT ( 'NONE',  ( -19.23287947355762384, -7.152392467615741545, 11.49999999999998934 ) ) ;
#59541=PLANE ( 'NONE',  #86797 ) ;
#59542=CARTESIAN_POINT ( 'NONE',  ( -55.52287095715005449, -24.99132157543083821, 2.256160258750667502 ) ) ;
#59543=CARTESIAN_POINT ( 'NONE',  ( -78.62287095715005592, -29.50250786944525672, 11.44777988621623521 ) ) ;
#59544=ORIENTED_EDGE ( 'NONE', *, *, #89286, .F. ) ;
#59548=B_SPLINE_CURVE_WITH_KNOTS ( 'NONE', 3,
 ( #31289, #62256, #16056, #24174, #55148, #16554 ),
 .UNSPECIFIED., .F., .F.,
 ( 4, 2, 4 ),
 ( 0.000000000000000000, 0.001380901958385383124, 0.002761803916770766247 ),
 .UNSPECIFIED. ) ;
#59549=VERTEX_POINT ( 'NONE', #68104 ) ;
#59550=VERTEX_POINT ( 'NONE', #29025 ) ;
#59551=CARTESIAN_POINT ( 'NONE',  ( -55.52287095715007581, -24.83602698348158810, 1.605859176311263070 ) ) ;
#59553=CARTESIAN_POINT ( 'NONE',  ( -76.63826584465937231, -23.96119346886880663, -0.6495511937832059157 ) ) ;
#59554=CARTESIAN_POINT ( 'NONE',  ( -4.563637348303267949, -20.04915943051449645, -1.500000000000002220 ) ) ;
#59555=ADVANCED_FACE ( 'NONE', ( #76679 ), #5692, .F. ) ;
#59556=CARTESIAN_POINT ( 'NONE',  ( -10.34410514300256523, -18.92461576200269491, 11.49999999999999645 ) ) ;
#59558=CARTESIAN_POINT ( 'NONE',  ( -49.92862301476790066, -25.14597343102002824, 7.027096283259375298 ) ) ;
#59559=CARTESIAN_POINT ( 'NONE',  ( -99.57239932359995294, -25.30502750817439761, 4.874438929701363499 ) ) ;
#59560=CARTESIAN_POINT ( 'NONE',  ( -35.52287095715005449, -23.48783264083451883, -1.443836473374936258 ) ) ;
#59561=CARTESIAN_POINT ( 'NONE',  ( 19.44376294880228428, 11.01865886811674677, 11.49999999999998934 ) ) ;
#59563=ADVANCED_FACE ( 'NONE', ( #6689 ), #92420, .F. ) ;
#59564=PLANE ( 'NONE',  #17300 ) ;
#59565=CARTESIAN_POINT ( 'NONE',  ( -61.58953762381672448, -24.64898659630528854, 1.056161002820822148 ) ) ;
#59566=VERTEX_POINT ( 'NONE', #53876 ) ;
#59567=EDGE_CURVE ( 'NONE', #13108, #90802, #88860, .T. ) ;
#59568=CARTESIAN_POINT ( 'NONE',  ( -94.52287095715001897, -24.34917612406837151, 0.1852690917426572381 ) ) ;
#59570=CARTESIAN_POINT ( 'NONE',  ( -2.496121100066326814, 20.73550571027955769, 11.49999999999998934 ) ) ;
#59571=ORIENTED_EDGE ( 'NONE', *, *, #37561, .T. ) ;
#59572=B_SPLINE_CURVE_WITH_KNOTS ( 'NONE', 3,
 ( #96268, #65842, #26753, #94757, #87658, #34370 ),
 .UNSPECIFIED., .F., .F.,
 ( 4, 2, 4 ),
 ( 1.570887131794638196E-05, 0.001396322306279761940, 0.002776935741241577573 ),
 .UNSPECIFIED. ) ;
#59573=CARTESIAN_POINT ( 'NONE',  ( -67.62364353413191509, -24.66019654487199730, 8.947790411086115725 ) ) ;
#59577=CARTESIAN_POINT ( 'NONE',  ( -50.38822539166533687, -25.30267106383720943, 4.736250553104468075 ) ) ;
#59578=CARTESIAN_POINT ( 'NONE',  ( 5.126256225908648823, -20.47799061884807870, -1.500000000000002220 ) ) ;
#59580=CARTESIAN_POINT ( 'NONE',  ( -34.52287095715006160, -24.64965694238575011, 8.947790433994207149 ) ) ;
#59581=CARTESIAN_POINT ( 'NONE',  ( -63.62287095715004881, -23.48786465467241058, 11.44779295918254824 ) ) ;
#59584=CARTESIAN_POINT ( 'NONE',  ( -76.59623078494088588, -23.96169478059713143, 10.65365249895718058 ) ) ;
#59585=FACE_OUTER_BOUND ( 'NONE', #54189, .T. ) ;
#59586=CARTESIAN_POINT ( 'NONE',  ( -19.25911440464646063, 10.06369110047026538, -1.500000000000002220 ) ) ;
#59587=LINE ( 'NONE', #98117, #12256 ) ;
#59588=CARTESIAN_POINT ( 'NONE',  ( 18.42719714020066846, 12.55551944762973626, 11.49999999999999645 ) ) ;
#59590=CARTESIAN_POINT ( 'NONE',  ( -33.52287095715006160, -24.51283580621449687, 0.6167428607045510880 ) ) ;
#59592=CARTESIAN_POINT ( 'NONE',  ( -106.5228709571500758, -23.47596703998600631, 11.44779298504228038 ) ) ;
#59593=VERTEX_POINT ( 'NONE', #21895 ) ;
#59594=ORIENTED_EDGE ( 'NONE', *, *, #7401, .F. ) ;
#59595=EDGE_LOOP ( 'NONE', ( #86218, #4394, #197, #96997 ) ) ;
#59596=CARTESIAN_POINT ( 'NONE',  ( -75.52287095715011844, -23.48783264082477373, -1.443836473390087694 ) ) ;
#59598=CARTESIAN_POINT ( 'NONE',  ( -78.94388818075310610, -25.03137962884571266, 6.014208626624816922 ) ) ;
#59599=CARTESIAN_POINT ( 'NONE',  ( -67.52287095715006160, -23.48786465467241769, 11.44779295918254647 ) ) ;
#59600=CARTESIAN_POINT ( 'NONE',  ( -2.960655606634402748, -19.13016773636607581, -1.500000000000002220 ) ) ;
#59604=CARTESIAN_POINT ( 'NONE',  ( -18.68205546197936684, -5.105407162728520021, 11.49999999999999645 ) ) ;
#59606=EDGE_LOOP ( 'NONE', ( #96975, #51562, #22348, #33200 ) ) ;
#59611=FACE_OUTER_BOUND ( 'NONE', #20490, .T. ) ;
#59612=B_SPLINE_CURVE_WITH_KNOTS ( 'NONE', 3,
 ( #36872, #14016, #29756, #36372 ),
 .UNSPECIFIED., .F., .F.,
 ( 4, 4 ),
 ( 0.000000000000000000, 0.9302372224392947420 ),
 .UNSPECIFIED. ) ;
#59613=CARTESIAN_POINT ( 'NONE',  ( 15.22544387773384500, -12.34335808662847178, 11.49999999999998934 ) ) ;
#59614=B_SPLINE_SURFACE_WITH_KNOTS ( 'NONE', 3, 3, ( 
 ( #88796, #83657, #59843, #100359 ),
 ( #68940, #76531, #45611, #6544 ),
 ( #44608, #36486, #37491, #67451 ),
 ( #52225, #99379, #14139, #98376 ),
 ( #28880, #90781, #21251, #30372 ),
 ( #61344, #75040, #13140, #91276 ),
 ( #7038, #51724, #37990, #5535 ) ),
 .UNSPECIFIED., .F., .F., .F.,
 ( 4, 3, 4 ),
 ( 4, 4 ),
 ( 0.0004766839783815509496, 0.1029713700210891786, 0.2054660560637968092 ),
 ( 0.6596618039411151768, 0.6609788952414030749 ),
 .UNSPECIFIED. ) ;
#59617=CARTESIAN_POINT ( 'NONE',  ( -0.8629811567608781653, -21.54619324973139172, 11.49999999999998934 ) ) ;
#59618=CARTESIAN_POINT ( 'NONE',  ( -32.62287095715004881, -29.50248528299804818, 1.056150453629029817 ) ) ;
#59619=DIRECTION ( 'NONE',  ( -3.773278334453079618E-23, 0.9999999999976377785, 2.173523156925979975E-06 ) ) ;
#59620=CARTESIAN_POINT ( 'NONE',  ( -81.58953762381669605, -24.64965694238407323, 8.947790433994653014 ) ) ;
#59621=CARTESIAN_POINT ( 'NONE',  ( -99.92039718326317654, -25.18439361145108180, 3.410800908530512654 ) ) ;
#59622=CARTESIAN_POINT ( 'NONE',  ( -12.06219892284564388, 19.56905390912838172, -1.500000000000002220 ) ) ;
#59625=CARTESIAN_POINT ( 'NONE',  ( -118.5228709571500758, -24.64965694238408034, 8.947790433994191162 ) ) ;
#59626=FACE_OUTER_BOUND ( 'NONE', #59796, .T. ) ;
#59627=CARTESIAN_POINT ( 'NONE',  ( 13.66866334921533799, -14.80927461459226890, 11.49999999999999645 ) ) ;
#59628=CARTESIAN_POINT ( 'NONE',  ( -70.62287095715005592, -23.47593901973091235, -1.443836447539006196 ) ) ;
#59629=PLANE ( 'NONE',  #61408 ) ;
#59632=CARTESIAN_POINT ( 'NONE',  ( -76.62287095715007013, -29.50248528299804818, 1.056150453629038477 ) ) ;
#59633=CARTESIAN_POINT ( 'NONE',  ( -75.52287095715006160, -24.99132157543084176, 2.256160258750667502 ) ) ;
#59634=CARTESIAN_POINT ( 'NONE',  ( -17.31707178780640533, -9.736581320607820444, 11.49999999999998934 ) ) ;
#59635=CARTESIAN_POINT ( 'NONE',  ( -113.6295937444302524, -23.73766607897670156, -1.055555164236448240 ) ) ;
#59637=CARTESIAN_POINT ( 'NONE',  ( 12.99534586470982234, -14.87506298573330632, -1.500000000000002220 ) ) ;
#59638=EDGE_CURVE ( 'NONE', #44200, #32974, #23393, .T. ) ;
#59640=CARTESIAN_POINT ( 'NONE',  ( -126.5215128601554255, -23.96169478059714208, 10.65365249895716637 ) ) ;
#59641=EDGE_CURVE ( 'NONE', #89889, #82876, #20242, .T. ) ;
#59643=CARTESIAN_POINT ( 'NONE',  ( -125.6228709571500843, -24.91570333823101180, 8.075032458375559941 ) ) ;
#59644=CARTESIAN_POINT ( 'NONE',  ( -94.62287095715005592, -29.50250243563736774, 8.947779886222139822 ) ) ;
#59645=CARTESIAN_POINT ( 'NONE',  ( 19.89799572200132971, -5.707369160466581270, 11.49999999999999645 ) ) ;
#59647=AXIS2_PLACEMENT_3D ( 'NONE', #37701, #6252, #35720 ) ;
#59649=DIRECTION ( 'NONE',  ( 0.000000000000000000, -2.173523156925979552E-06, 0.9999999999976378895 ) ) ;
#59650=CARTESIAN_POINT ( 'NONE',  ( 22.61316900856233403, 2.020702135111208442, 11.49999999999999645 ) ) ;
#59655=EDGE_CURVE ( 'NONE', #11783, #66705, #16238, .T. ) ;
#59656=CARTESIAN_POINT ( 'NONE',  ( -63.57960882203882136, -24.65952944569304250, 1.056160979905695463 ) ) ;
#59660=ADVANCED_FACE ( 'NONE', ( #6022 ), #43598, .T. ) ;
#59661=CARTESIAN_POINT ( 'NONE',  ( -99.30666603356964117, -25.23741546797077362, 6.288603370249809643 ) ) ;
#59662=CARTESIAN_POINT ( 'NONE',  ( 4.181975289622855918, -22.47981636197143374, 11.49999999999998934 ) ) ;
#59663=CARTESIAN_POINT ( 'NONE',  ( -29.55259386707723124, -23.87806136140024194, -0.6495508823503305385 ) ) ;
#59664=CARTESIAN_POINT ( 'NONE',  ( 14.45009471711328786, 16.04676183837579373, -1.500000000000002220 ) ) ;
#59668=CARTESIAN_POINT ( 'NONE',  ( 9.831018646898828095, -20.30805102056165623, 11.49999999999999645 ) ) ;
#59670=CARTESIAN_POINT ( 'NONE',  ( -70.13845683480205651, -25.31612421240863142, 4.855284239541365565 ) ) ;
#59671=CARTESIAN_POINT ( 'NONE',  ( 8.537626919312410578, 20.26776412955123163, 11.49999999999998934 ) ) ;
#59673=CARTESIAN_POINT ( 'NONE',  ( -105.6271209236252275, -24.63419186844610920, 9.035850630976920428 ) ) ;
#59674=CARTESIAN_POINT ( 'NONE',  ( -41.58766378979927936, -25.29087150074615309, 3.364589589010316573 ) ) ;
#59676=CARTESIAN_POINT ( 'NONE',  ( -89.62287095715004170, -23.48786465467241413, 11.44779295918254114 ) ) ;
#59677=CARTESIAN_POINT ( 'NONE',  ( -90.50788615195934028, -24.40133493613049964, 9.663955038902805939 ) ) ;
#59679=CARTESIAN_POINT ( 'NONE',  ( -49.62287095715005592, -23.48786465467241058, 11.44779295918254824 ) ) ;
#59680=ORIENTED_EDGE ( 'NONE', *, *, #36840, .T. ) ;
#59683=CARTESIAN_POINT ( 'NONE',  ( -104.5228709571501327, -24.34917612406838572, 0.1852690917426617068 ) ) ;
#59684=CARTESIAN_POINT ( 'NONE',  ( -36.51286536810861350, -23.73766607897670156, -1.055555164236459120 ) ) ;
#59685=CARTESIAN_POINT ( 'NONE',  ( 7.241121213506172438, 19.11196469071355963, -1.500000000000002220 ) ) ;
#59686=EDGE_CURVE ( 'NONE', #2769, #11988, #32733, .T. ) ;
#59689=CARTESIAN_POINT ( 'NONE',  ( -30.56688274934923655, -25.56688301298833821, 3.825958421598584014 ) ) ;
#59690=ADVANCED_FACE ( 'NONE', ( #92750 ), #38479, .F. ) ;
#59691=DIRECTION ( 'NONE',  ( -1.000000000000000000, -3.773278334444166432E-23, -8.201307841325785021E-29 ) ) ;
#59694=PLANE ( 'NONE',  #14408 ) ;
#59696=CARTESIAN_POINT ( 'NONE',  ( -6.767879454864726974, -19.68250801024624508, 11.49999999999998934 ) ) ;
#59698=ORIENTED_EDGE ( 'NONE', *, *, #6101, .F. ) ;
#59701=B_SPLINE_SURFACE_WITH_KNOTS ( 'NONE', 3, 3, ( 
 ( #86639, #55712, #46587, #31352 ),
 ( #9515, #55211, #39965, #67547 ),
 ( #906, #401, #39469, #38961 ),
 ( #54704, #62316, #85133, #75628 ),
 ( #29459, #98465, #31860, #69916 ),
 ( #94247, #9015, #70929, #44703 ),
 ( #85636, #1416, #32351, #78510 ) ),
 .UNSPECIFIED., .F., .F., .F.,
 ( 4, 3, 4 ),
 ( 4, 4 ),
 ( 0.7945040050992231428, 0.8970133687736494554, 0.9995227324480756570 ),
 ( 0.1895421625358439111, 0.1906423923308985524 ),
 .UNSPECIFIED. ) ;
#59703=CARTESIAN_POINT ( 'NONE',  ( -33.52287095715006160, -23.47593901973090169, -1.443836447538997314 ) ) ;
#59704=VERTEX_POINT ( 'NONE', #45598 ) ;
#59705=ORIENTED_EDGE ( 'NONE', *, *, #81643, .F. ) ;
#59708=CARTESIAN_POINT ( 'NONE',  ( -60.62287095715005592, -23.48786465467241058, 11.44779295918254824 ) ) ;
#59709=CARTESIAN_POINT ( 'NONE',  ( -70.74035176281489612, -25.24515055801344587, 5.376056033097980524 ) ) ;
#59710=CARTESIAN_POINT ( 'NONE',  ( 19.07224962250127831, -11.27678277851665634, 11.49999999999999645 ) ) ;
#59712=B_SPLINE_CURVE_WITH_KNOTS ( 'NONE', 3,
 ( #55319, #1018, #70025, #61925, #31464, #39578 ),
 .UNSPECIFIED., .F., .F.,
 ( 4, 2, 4 ),
 ( 0.000000000000000000, 0.001380901958385389195, 0.002761803916770778390 ),
 .UNSPECIFIED. ) ;
#59713=CARTESIAN_POINT ( 'NONE',  ( -108.5942885673410672, -23.73766607897671932, -1.055555164236429366 ) ) ;
#59714=CARTESIAN_POINT ( 'NONE',  ( -7.157701736792966507, -21.45640540170154509, -1.500000000000002220 ) ) ;
#59717=CARTESIAN_POINT ( 'NONE',  ( -88.62287095715004170, -29.50247984919015209, -1.443849546365051806 ) ) ;
#59719=ORIENTED_EDGE ( 'NONE', *, *, #35373, .T. ) ;
#59720=B_SPLINE_CURVE_WITH_KNOTS ( 'NONE', 3,
 ( #53981, #29629, #38234, #6785 ),
 .UNSPECIFIED., .F., .F.,
 ( 4, 4 ),
 ( 0.000000000000000000, 9.999999999998897304E-05 ),
 .UNSPECIFIED. ) ;
#59722=CARTESIAN_POINT ( 'NONE',  ( -11.83016301840747175, -16.26703346747452983, 11.49999999999998934 ) ) ;
#59723=CARTESIAN_POINT ( 'NONE',  ( -57.51495926866731168, -23.73791477778911840, 11.05961554403170588 ) ) ;
#59725=VECTOR ( 'NONE', #13805, 1000.000000000000114 ) ;
#59726=CARTESIAN_POINT ( 'NONE',  ( -40.25541618970063240, -25.29345417698259624, 5.538673509577355603 ) ) ;
#59727=CARTESIAN_POINT ( 'NONE',  ( -3.941980378682776287, 21.93750326593198352, -1.500000000000002220 ) ) ;
#59729=EDGE_LOOP ( 'NONE', ( #48206, #5969, #21020, #47833 ) ) ;
#59731=DIRECTION ( 'NONE',  ( 0.000000000000000000, 0.9999999999976377785, 2.173523156925979975E-06 ) ) ;
#59732=CARTESIAN_POINT ( 'NONE',  ( -27.61175609890311478, -24.59808689224374589, 1.630391722295341461 ) ) ;
#59733=CARTESIAN_POINT ( 'NONE',  ( -111.5895376238167245, -24.65952944569304606, 1.056160979905705455 ) ) ;
#59734=CARTESIAN_POINT ( 'NONE',  ( -129.5228709571500474, -24.66019654487199730, 8.947790411086115725 ) ) ;
#59735=CARTESIAN_POINT ( 'NONE',  ( -19.08498223313328168, 4.104482590468319536, -1.500000000000002220 ) ) ;
#59737=CARTESIAN_POINT ( 'NONE',  ( -21.39523464106120088, -1.845724655749456433, 11.49999999999998934 ) ) ;
#59739=CARTESIAN_POINT ( 'NONE',  ( -120.5228709571500332, -24.15431212366390312, -0.2830839119429085504 ) ) ;
#59740=CARTESIAN_POINT ( 'NONE',  ( -125.6228709571500843, -25.00182538069146432, 7.747789668545100206 ) ) ;
#59741=CARTESIAN_POINT ( 'NONE',  ( 13.80103769381473811, 18.14473668730428813, -1.500000000000002220 ) ) ;
#59742=B_SPLINE_CURVE_WITH_KNOTS ( 'NONE', 3,
 ( #3779, #48952, #42353, #88008, #73285, #32710 ),
 .UNSPECIFIED., .F., .F.,
 ( 4, 2, 4 ),
 ( 6.384118678611711726E-06, 0.001386860460828375418, 0.002767336802978138856 ),
 .UNSPECIFIED. ) ;
#59744=CARTESIAN_POINT ( 'NONE',  ( -106.5572848214566477, -23.73791477778912551, 11.05961554403169700 ) ) ;
#59746=CARTESIAN_POINT ( 'NONE',  ( 16.79105032741591330, -10.77411451815220822, 11.49999999999999645 ) ) ;
#59747=CARTESIAN_POINT ( 'NONE',  ( -118.5228709571501184, -24.66019654487200441, 8.947790411086110396 ) ) ;
#59748=ADVANCED_FACE ( 'NONE', ( #99365 ), #94633, .F. ) ;
#59749=EDGE_CURVE ( 'NONE', #33110, #5456, #87022, .T. ) ;
#59750=CARTESIAN_POINT ( 'NONE',  ( -57.55620429048338593, -23.48786465467241413, 11.44779295918254824 ) ) ;
#59751=DIRECTION ( 'NONE',  ( -1.000000000000000000, -3.773278334444167608E-23, -8.201307833595939069E-29 ) ) ;
#59753=CARTESIAN_POINT ( 'NONE',  ( -26.49745401032653191, -24.63815014598046460, 2.058893537102744364 ) ) ;
#59754=CARTESIAN_POINT ( 'NONE',  ( -59.52287095715006160, -24.65952944569304961, 1.056160979905695463 ) ) ;
#59755=EDGE_CURVE ( 'NONE', #66631, #3013, #51285, .T. ) ;
#59756=CARTESIAN_POINT ( 'NONE',  ( 14.84582651547613352, 15.88809324551894520, 11.49999999999998934 ) ) ;
#59758=CARTESIAN_POINT ( 'NONE',  ( 19.11985901488480621, -4.296470200863222288, -1.500000000000002220 ) ) ;
#59760=CARTESIAN_POINT ( 'NONE',  ( -69.52287095715006160, -29.50250243563736774, 8.947779886222143375 ) ) ;
#59761=VERTEX_POINT ( 'NONE', #53214 ) ;
#59765=CARTESIAN_POINT ( 'NONE',  ( 10.21088607376515789, 17.76353854702842483, 11.49999999999999645 ) ) ;
#59766=CARTESIAN_POINT ( 'NONE',  ( -47.52287095715006870, -23.73934037231757088, 11.05740245334329508 ) ) ;
#59767=B_SPLINE_CURVE_WITH_KNOTS ( 'NONE', 3,
 ( #61704, #92628, #13505, #23106 ),
 .UNSPECIFIED., .F., .F.,
 ( 4, 4 ),
 ( 0.000000000000000000, 9.999999999997510880E-05 ),
 .UNSPECIFIED. ) ;
#59768=CARTESIAN_POINT ( 'NONE',  ( -40.62287095715005592, -23.48783264082478084, -1.443836473390072817 ) ) ;
#59769=EDGE_CURVE ( 'NONE', #24728, #29559, #9394, .T. ) ;
#59771=CARTESIAN_POINT ( 'NONE',  ( -117.6228709571500559, -29.50247984919015209, -1.443849546365046699 ) ) ;
#59773=AXIS2_PLACEMENT_3D ( 'NONE', #4617, #51784, #66539 ) ;
#59774=CARTESIAN_POINT ( 'NONE',  ( -78.62287095715005592, -23.94994826722515668, -0.6494450866351704210 ) ) ;
#59775=VECTOR ( 'NONE', #11856, 1000.000000000000114 ) ;
#59776=CARTESIAN_POINT ( 'NONE',  ( -49.52287095715006160, -29.50247984919015209, -1.443849546365058689 ) ) ;
#59779=VECTOR ( 'NONE', #20723, 1000.000000000000114 ) ;
#59780=CARTESIAN_POINT ( 'NONE',  ( -7.156825135384894843, 21.90021990432103038, 11.49999999999999645 ) ) ;
#59781=CARTESIAN_POINT ( 'NONE',  ( -15.20078144808659992, 16.97451310947862169, -1.500000000000002220 ) ) ;
#59786=B_SPLINE_CURVE_WITH_KNOTS ( 'NONE', 3,
 ( #33325, #26725, #65320, #8121, #499, #4, #31451, #61915, #96241, #92840, #17610, #23323, #54308, #2904, #85234, #15722 ),
 .UNSPECIFIED., .F., .F.,
 ( 4, 2, 2, 2, 2, 2, 2, 4 ),
 ( 0.000000000000000000, 0.0001736386538236284779, 0.0003472773076472569559, 0.0006945546152945145622, 0.0008681932691181433112, 0.001041831922941772277, 0.001215470576765400809, 0.001389109230589029775 ),
 .UNSPECIFIED. ) ;
#59787=CARTESIAN_POINT ( 'NONE',  ( -108.8968792378191921, -25.05712065398430966, 7.447789548358837663 ) ) ;
#59788=CARTESIAN_POINT ( 'NONE',  ( -110.5124727292759985, -24.73486907724917572, 1.287355809206965240 ) ) ;
#59789=CARTESIAN_POINT ( 'NONE',  ( -17.52905966558703454, -13.16386835867055716, 11.49999999999998934 ) ) ;
#59791=FACE_OUTER_BOUND ( 'NONE', #53088, .T. ) ;
#59792=CARTESIAN_POINT ( 'NONE',  ( -41.46611000704998418, -25.28830591450888932, 4.188173661249235735 ) ) ;
#59793=CARTESIAN_POINT ( 'NONE',  ( -86.62287095715004170, -29.50250786944525672, 11.44777988621623344 ) ) ;
#59794=DIRECTION ( 'NONE',  ( -3.773278334453079030E-23, 0.9999999999976377785, 2.173523156925979128E-06 ) ) ;
#59795=CARTESIAN_POINT ( 'NONE',  ( -101.3738023147422780, -29.50249165161862663, 3.986241424695394109 ) ) ;
#59796=EDGE_LOOP ( 'NONE', ( #65453, #21606, #91156, #2269 ) ) ;
#59798=CARTESIAN_POINT ( 'NONE',  ( 5.028806042385554953, -19.83023610923392610, -1.500000000000002220 ) ) ;
#59799=ORIENTED_EDGE ( 'NONE', *, *, #29676, .F. ) ;
#59801=EDGE_LOOP ( 'NONE', ( #8517, #6365, #15714, #24483 ) ) ;
#59803=CARTESIAN_POINT ( 'NONE',  ( 21.75825945658488436, -7.631246777643061030, 11.49999999999998934 ) ) ;
#59804=CARTESIAN_POINT ( 'NONE',  ( -95.55620429048339304, -25.00158670708909980, 2.256160236439165967 ) ) ;
#59805=CARTESIAN_POINT ( 'NONE',  ( -18.82339984186270598, 7.397194320553815317, -1.500000000000002220 ) ) ;
#59806=ORIENTED_EDGE ( 'NONE', *, *, #22607, .T. ) ;
#59808=CARTESIAN_POINT ( 'NONE',  ( -41.86767815140794369, -25.29562010035766662, 4.300008416864591787 ) ) ;
#59809=EDGE_CURVE ( 'NONE', #77123, #97163, #17503, .T. ) ;
#59810=CARTESIAN_POINT ( 'NONE',  ( -101.5228709571500900, -24.66019654487200441, 8.947790411086119278 ) ) ;
#59811=CARTESIAN_POINT ( 'NONE',  ( -70.62989412486773233, -24.73486907724917572, 1.287355809206963908 ) ) ;
#59812=CARTESIAN_POINT ( 'NONE',  ( -2.751442626040462081, 21.25944542233241563, 11.49999999999999645 ) ) ;
#59814=CARTESIAN_POINT ( 'NONE',  ( -61.62287095715004881, -29.50250243563736774, 8.947779886222145151 ) ) ;
#59815=ORIENTED_EDGE ( 'NONE', *, *, #44583, .F. ) ;
#59816=CARTESIAN_POINT ( 'NONE',  ( 2.909938941155331360, -20.50406750007545398, -1.500000000000002220 ) ) ;
#59823=ORIENTED_EDGE ( 'NONE', *, *, #94734, .F. ) ;
#59824=CARTESIAN_POINT ( 'NONE',  ( -20.94189920129180038, 1.864940847883316488, -1.500000000000002220 ) ) ;
#59825=CARTESIAN_POINT ( 'NONE',  ( -15.01370250125036421, 16.05796621403891677, 11.49999999999999645 ) ) ;
#59826=FACE_OUTER_BOUND ( 'NONE', #19123, .T. ) ;
#59827=CARTESIAN_POINT ( 'NONE',  ( -0.06565682164858396841, -22.51586213336150166, -1.500000000000002220 ) ) ;
#59828=CARTESIAN_POINT ( 'NONE',  ( 0.9685562702117149758, 20.96446713366763248, 11.49999999999998934 ) ) ;
#59830=CARTESIAN_POINT ( 'NONE',  ( -72.62287095715008434, -24.50216790748099527, 0.6166512839513557109 ) ) ;
#59831=CARTESIAN_POINT ( 'NONE',  ( -53.62287095715004881, -23.48786465467241058, 11.44779295918255002 ) ) ;
#59835=FACE_OUTER_BOUND ( 'NONE', #36574, .T. ) ;
#59837=CARTESIAN_POINT ( 'NONE',  ( 15.25824911148008844, 15.06768998368162471, -1.500000000000002220 ) ) ;
#59839=ORIENTED_EDGE ( 'NONE', *, *, #44755, .F. ) ;
#59840=CARTESIAN_POINT ( 'NONE',  ( -12.37649675270136918, 17.12833386298736471, 11.49999999999998934 ) ) ;
#59843=CARTESIAN_POINT ( 'NONE',  ( -64.56596238235714225, -23.48783264082477018, -1.443836473390096353 ) ) ;
#59845=CARTESIAN_POINT ( 'NONE',  ( -83.50633554728430852, -24.35071581493543036, 9.817618358456028815 ) ) ;
#59846=FACE_OUTER_BOUND ( 'NONE', #7090, .T. ) ;
#59848=CARTESIAN_POINT ( 'NONE',  ( 22.02032638543937182, 1.892999326154024553, -1.500000000000002220 ) ) ;
#59849=B_SPLINE_CURVE_WITH_KNOTS ( 'NONE', 3,
 ( #4834, #36287, #28666, #29160 ),
 .UNSPECIFIED., .F., .F.,
 ( 4, 4 ),
 ( 0.000000000000000000, 9.999999999998897304E-05 ),
 .UNSPECIFIED. ) ;
#59850=FACE_OUTER_BOUND ( 'NONE', #380, .T. ) ;
#59852=CARTESIAN_POINT ( 'NONE',  ( -34.22287095715005734, -23.47593901973090169, -1.443836447538998202 ) ) ;
#59853=PLANE ( 'NONE',  #46867 ) ;
#59854=AXIS2_PLACEMENT_3D ( 'NONE', #57079, #94617, #89013 ) ;
#59855=CARTESIAN_POINT ( 'NONE',  ( -100.5179258051187787, -23.85016227208580375, -0.8807180028928297544 ) ) ;
#59857=CARTESIAN_POINT ( 'NONE',  ( 3.148799746435844593, 19.17640706095922098, 11.49999999999998934 ) ) ;
#59858=VECTOR ( 'NONE', #37053, 1000.000000000000114 ) ;
#59859=CARTESIAN_POINT ( 'NONE',  ( 12.64048258313813733, 17.25876517447949610, -1.500000000000002220 ) ) ;
#59860=LINE ( 'NONE', #44625, #35316 ) ;
#59861=CARTESIAN_POINT ( 'NONE',  ( -68.62287095715005592, -29.50250786944525672, 11.44777988621623699 ) ) ;
#59862=CARTESIAN_POINT ( 'NONE',  ( -72.52287095715007581, -24.50321055353804667, 9.387540953477529371 ) ) ;
#59863=CARTESIAN_POINT ( 'NONE',  ( -128.9228709571500815, -23.47593901973090524, -1.443836447538996204 ) ) ;
#59864=B_SPLINE_CURVE_WITH_KNOTS ( 'NONE', 3,
 ( #99372, #59327, #60344, #35984, #44103, #75529 ),
 .UNSPECIFIED., .F., .F.,
 ( 4, 2, 4 ),
 ( 1.570887131794795405E-05, 0.001396322306279761940, 0.002776935741241575838 ),
 .UNSPECIFIED. ) ;
#59865=CARTESIAN_POINT ( 'NONE',  ( -14.08738070862771963, 17.71811851510361535, -1.500000000000002220 ) ) ;
#59868=CARTESIAN_POINT ( 'NONE',  ( -40.92287095715006018, -23.47596703998600276, 11.44779298504227683 ) ) ;
#59869=CARTESIAN_POINT ( 'NONE',  ( 18.78060722631472501, -6.265068672152646734, 11.49999999999999645 ) ) ;
#59871=EDGE_CURVE ( 'NONE', #50459, #79998, #34401, .T. ) ;
#59872=CARTESIAN_POINT ( 'NONE',  ( -35.55620429048339304, -25.00158670708909270, 2.256160236439165967 ) ) ;
#59874=CARTESIAN_POINT ( 'NONE',  ( -53.62287095715004881, -24.65952944569303895, 1.056160979905692576 ) ) ;
#59875=CARTESIAN_POINT ( 'NONE',  ( -78.94303308397306296, -25.26612693627497208, 5.977536690229215743 ) ) ;
#59876=EDGE_CURVE ( 'NONE', #69684, #16998, #1696, .T. ) ;
#59878=CARTESIAN_POINT ( 'NONE',  ( -13.25059585359799108, -17.08168364658555305, -1.500000000000002220 ) ) ;
#59879=FACE_OUTER_BOUND ( 'NONE', #809, .T. ) ;
#59880=CARTESIAN_POINT ( 'NONE',  ( -101.5895376238167245, -23.48786465467242479, 11.44779295918254114 ) ) ;
#59882=DIRECTION ( 'NONE',  ( 0.000000000000000000, 0.9999999999976377785, 2.173523156925979128E-06 ) ) ;
#59883=PLANE ( 'NONE',  #31223 ) ;
#59884=CARTESIAN_POINT ( 'NONE',  ( -14.51517298184297289, -13.48802281452852725, 11.49999999999998934 ) ) ;
#59885=ORIENTED_EDGE ( 'NONE', *, *, #58278, .F. ) ;
#59887=CARTESIAN_POINT ( 'NONE',  ( 14.56535739210195857, -14.21638276092092745, 11.49999999999999645 ) ) ;
#59891=ORIENTED_EDGE ( 'NONE', *, *, #75986, .F. ) ;
#59892=B_SPLINE_SURFACE_WITH_KNOTS ( 'NONE', 3, 1, ( 
 ( #49624, #47621 ),
 ( #11049, #42013 ),
 ( #86167, #72956 ),
 ( #3452, #78538 ),
 ( #86665, #70956 ),
 ( #32382, #9543 ),
 ( #40505, #19149 ),
 ( #43988, #42513 ),
 ( #90166, #19645 ),
 ( #5424, #73451 ),
 ( #36376, #28765 ) ),
 .UNSPECIFIED., .F., .F., .F.,
 ( 4, 1, 1, 1, 1, 1, 1, 1, 4 ),
 ( 2, 2 ),
 ( 0.000000000000000000, 0.1192834503733694734, 0.2370928820686294958, 0.3547960442151275040, 0.4745763009408505706, 0.5974600658149772370, 0.7249261546156138269, 0.8588831991927623477, 1.000000000000000000 ),
 ( 0.000000000000000000, 1.000000000000000000 ),
 .UNSPECIFIED. ) ;
#59893=CARTESIAN_POINT ( 'NONE',  ( -102.5602270407120926, -23.48786465467241058, 11.44779295918254292 ) ) ;
#59895=CARTESIAN_POINT ( 'NONE',  ( -75.62287095715005592, -23.48783264082478084, -1.443836473390065489 ) ) ;
#59898=CARTESIAN_POINT ( 'NONE',  ( -1.290058840521481454, 20.04182742388497473, -1.500000000000002220 ) ) ;
#59899=EDGE_CURVE ( 'NONE', #79071, #30912, #59742, .T. ) ;
#59900=CARTESIAN_POINT ( 'NONE',  ( -79.55620429048342146, -23.47593901973091235, -1.443836447539004642 ) ) ;
#59903=CARTESIAN_POINT ( 'NONE',  ( 15.09361930729867574, -17.17024899132524496, 11.49999999999999645 ) ) ;
#59904=CARTESIAN_POINT ( 'NONE',  ( -49.51279233427662518, -25.31297074183165563, 4.076580152408665114 ) ) ;
#59910=CARTESIAN_POINT ( 'NONE',  ( -99.90881925540746522, -25.03707831087709934, 7.590867751134624974 ) ) ;
#59913=CARTESIAN_POINT ( 'NONE',  ( -0.9335293527496063559, -20.33857301660709638, -1.500000000000002220 ) ) ;
#59914=VERTEX_POINT ( 'NONE', #79382 ) ;
#59915=EDGE_CURVE ( 'NONE', #53379, #27734, #44105, .T. ) ;
#59916=CARTESIAN_POINT ( 'NONE',  ( 13.56796309060646166, -18.52494293750034871, -1.500000000000002220 ) ) ;
#59917=DIRECTION ( 'NONE',  ( 0.000000000000000000, 0.9999999999976377785, 2.173523156925979975E-06 ) ) ;
#59919=VECTOR ( 'NONE', #10283, 1000.000000000000114 ) ;
#59920=CARTESIAN_POINT ( 'NONE',  ( -49.10457154551148307, -25.26416398485831749, 3.999772271414141489 ) ) ;
#59924=CARTESIAN_POINT ( 'NONE',  ( -74.55620429048340725, -23.47593901973091235, -1.443836447539006196 ) ) ;
#59925=CARTESIAN_POINT ( 'NONE',  ( -20.48789480994130230, 5.740754632170482097, 11.49999999999999645 ) ) ;
#59926=ORIENTED_EDGE ( 'NONE', *, *, #89279, .T. ) ;
#59928=VERTEX_POINT ( 'NONE', #34717 ) ;
#59929=CARTESIAN_POINT ( 'NONE',  ( 9.107982344273736430, -20.20341329189913537, -1.500000000000002220 ) ) ;
#59930=CARTESIAN_POINT ( 'NONE',  ( -20.60850594246137035, -0.7621957659720622891, -1.500000000000002220 ) ) ;
#59932=ORIENTED_EDGE ( 'NONE', *, *, #85079, .T. ) ;
#59934=DIRECTION ( 'NONE',  ( -1.000000000000000000, -3.773278334444167608E-23, -8.201307833595939069E-29 ) ) ;
#59936=CARTESIAN_POINT ( 'NONE',  ( -121.6228709571500417, -23.48783264082478794, -1.443836473390058384 ) ) ;
#59938=ORIENTED_EDGE ( 'NONE', *, *, #70134, .T. ) ;
#59939=CARTESIAN_POINT ( 'NONE',  ( -49.52287095715007581, -23.95044443724991723, 10.65354141964649592 ) ) ;
#59940=FACE_OUTER_BOUND ( 'NONE', #61317, .T. ) ;
#59942=CARTESIAN_POINT ( 'NONE',  ( -16.75865769207039335, -12.26659692683164593, -1.500000000000002220 ) ) ;
#59943=CARTESIAN_POINT ( 'NONE',  ( 21.06710269851327766, -5.618397932909799941, 11.49999999999999645 ) ) ;
#59945=CARTESIAN_POINT ( 'NONE',  ( -50.60256128385139363, -25.03406269411437179, 7.557545390615620029 ) ) ;
#59947=CARTESIAN_POINT ( 'NONE',  ( -96.58953762381671027, -24.65952944569304606, 1.056160979905704123 ) ) ;
#59948=CARTESIAN_POINT ( 'NONE',  ( 20.43785579724129420, 9.289222182981756504, 11.49999999999998934 ) ) ;
#59949=FACE_OUTER_BOUND ( 'NONE', #18108, .T. ) ;
#59951=PLANE ( 'NONE',  #56667 ) ;
#59952=CARTESIAN_POINT ( 'NONE',  ( -51.70072539166533687, -25.26311289191998455, 3.987152081390995306 ) ) ;
#59954=VERTEX_POINT ( 'NONE', #27104 ) ;
#59955=CARTESIAN_POINT ( 'NONE',  ( -99.63657171274012114, -25.30666370342169813, 5.471494451533469139 ) ) ;
#59957=VERTEX_POINT ( 'NONE', #79881 ) ;
#59958=CARTESIAN_POINT ( 'NONE',  ( -16.96849063341007380, -12.82450338531451450, -1.500000000000002220 ) ) ;
#59961=CARTESIAN_POINT ( 'NONE',  ( -14.15979099334852798, -15.53166555317341135, -1.500000000000002220 ) ) ;
#59963=CARTESIAN_POINT ( 'NONE',  ( -11.11902432501355342, 19.77583997595719367, 11.49999999999998934 ) ) ;
#59964=CARTESIAN_POINT ( 'NONE',  ( -41.46611000704998418, -25.18431065692472615, 4.188173887285336683 ) ) ;
#59966=CARTESIAN_POINT ( 'NONE',  ( 6.492371748702247203, -20.92784845389783399, -1.500000000000002220 ) ) ;
#59967=CARTESIAN_POINT ( 'NONE',  ( -62.62287095715004881, -23.47596703998600276, 11.44779298504227505 ) ) ;
#59970=DIRECTION ( 'NONE',  ( -1.000000000000000000, -3.773278334444167608E-23, -8.201307833595939069E-29 ) ) ;
#59971=CARTESIAN_POINT ( 'NONE',  ( -130.5728709571500872, -25.14081846633249739, 7.291654623549849390 ) ) ;
#59972=CARTESIAN_POINT ( 'NONE',  ( -46.62287095715004881, -29.50250243563736774, 8.947779886222146928 ) ) ;
#59973=B_SPLINE_CURVE_WITH_KNOTS ( 'NONE', 3,
 ( #94466, #10232, #77720, #33074 ),
 .UNSPECIFIED., .F., .F.,
 ( 4, 4 ),
 ( 0.000000000000000000, 0.0001000000000000028644 ),
 .UNSPECIFIED. ) ;
#59974=CARTESIAN_POINT ( 'NONE',  ( -9.505907188867841029, -19.02311915605711690, -1.500000000000002220 ) ) ;
#59975=CARTESIAN_POINT ( 'NONE',  ( -112.6256797069762143, -24.34968618360934656, 0.1864209137779000991 ) ) ;
#59978=CARTESIAN_POINT ( 'NONE',  ( -85.50025541002817420, -24.73486907724917927, 1.287355809206964796 ) ) ;
#59979=CARTESIAN_POINT ( 'NONE',  ( -114.5228709571500616, -24.65952944569305316, 1.056160979905704123 ) ) ;
#59980=CARTESIAN_POINT ( 'NONE',  ( -90.55620429048337883, -24.99132157543166599, 2.256160258750667058 ) ) ;
#59981=ORIENTED_EDGE ( 'NONE', *, *, #70564, .F. ) ;
#59982=CARTESIAN_POINT ( 'NONE',  ( -119.6228709571500417, -24.65952944569304961, 1.056160979905704789 ) ) ;
#59983=CARTESIAN_POINT ( 'NONE',  ( 14.19269941865516671, -13.59168563846684563, 11.49999999999999645 ) ) ;
#59984=CARTESIAN_POINT ( 'NONE',  ( -78.52287095715006160, -23.48786465467241769, 11.44779295918254469 ) ) ;
#59987=CARTESIAN_POINT ( 'NONE',  ( -119.6228709571500559, -23.47593901973091235, -1.443836447538997536 ) ) ;
#59988=VERTEX_POINT ( 'NONE', #65197 ) ;
#59989=CARTESIAN_POINT ( 'NONE',  ( -55.62287095715005592, -29.50250786944525672, 11.44777988621623876 ) ) ;
#59990=CARTESIAN_POINT ( 'NONE',  ( -44.62287095715004881, -24.65952944569303895, 1.056160979905693686 ) ) ;
#59992=CARTESIAN_POINT ( 'NONE',  ( -26.97977519014201064, -24.63279798339582172, 8.111117997598707774 ) ) ;
#59993=CARTESIAN_POINT ( 'NONE',  ( -40.62287095715004170, -24.91570333823099048, 8.075032458375556388 ) ) ;
#59994=CARTESIAN_POINT ( 'NONE',  ( -18.83419513347712737, -5.836681878196540829, 11.49999999999998934 ) ) ;
#59995=VECTOR ( 'NONE', #34362, 1000.000000000000227 ) ;
#59996=ORIENTED_EDGE ( 'NONE', *, *, #60899, .T. ) ;
#59997=EDGE_CURVE ( 'NONE', #48335, #96746, #76782, .T. ) ;
#59998=AXIS2_PLACEMENT_3D ( 'NONE', #17083, #76969, #63285 ) ;
#59999=CARTESIAN_POINT ( 'NONE',  ( -33.62287095715005592, -29.50250786944525672, 11.44777988621624409 ) ) ;
#60000=CARTESIAN_POINT ( 'NONE',  ( -70.62287095715004170, -24.15431212366388891, -0.2830839119429064410 ) ) ;
#60002=AXIS2_PLACEMENT_3D ( 'NONE', #5176, #27023, #90413 ) ;
#60005=CARTESIAN_POINT ( 'NONE',  ( -54.52287095715006870, -24.50321055353805377, 9.387540953477524042 ) ) ;
#60008=CARTESIAN_POINT ( 'NONE',  ( -55.64123101047048436, -24.40034930558990922, 0.3402023900116022959 ) ) ;
#60009=CARTESIAN_POINT ( 'NONE',  ( -50.52287095715006160, -24.99156044556120193, 7.747789690856173195 ) ) ;
#60010=CARTESIAN_POINT ( 'NONE',  ( -31.62287095715005236, -23.47596703998600276, 11.44779298504227505 ) ) ;
#60011=CARTESIAN_POINT ( 'NONE',  ( -70.06086327669997615, -25.31201598263180941, 5.348962284489573449 ) ) ;
#60012=CARTESIAN_POINT ( 'NONE',  ( -91.52287095715006160, -24.50321055353804667, 9.387540953477515160 ) ) ;
#60013=CARTESIAN_POINT ( 'NONE',  ( -19.59816365915598979, -3.832847594873297403, 11.49999999999998934 ) ) ;
#60014=EDGE_CURVE ( 'NONE', #46913, #70257, #96120, .T. ) ;
#60015=CARTESIAN_POINT ( 'NONE',  ( -125.6228709571500843, -24.52323809116984776, 9.355190652339411272 ) ) ;
#60017=EDGE_LOOP ( 'NONE', ( #66304, #35880, #47166, #81976 ) ) ;
#60018=CARTESIAN_POINT ( 'NONE',  ( -63.52287095715006160, -23.72747288104470087, -1.053458166803227014 ) ) ;
#60022=CARTESIAN_POINT ( 'NONE',  ( -28.55620429048340725, -24.49093714213148232, 1.056161671301197424 ) ) ;
#60023=CARTESIAN_POINT ( 'NONE',  ( -39.63466154761483295, -24.34968618360933235, 0.1864209137778788383 ) ) ;
#60024=CARTESIAN_POINT ( 'NONE',  ( -76.52287095715007581, -29.50247984919015209, -1.443849546365053582 ) ) ;
#60027=B_SPLINE_CURVE_WITH_KNOTS ( 'NONE', 3,
 ( #72526, #74018, #19710, #3019, #12103, #82124, #95352, #4513 ),
 .UNSPECIFIED., .F., .F.,
 ( 4, 2, 2, 4 ),
 ( 6.384118678609614472E-06, 0.002007151183507257988, 0.003007534715921583810, 0.004007918248335909199 ),
 .UNSPECIFIED. ) ;
#60028=LINE ( 'NONE', #82838, #64129 ) ;
#60029=CARTESIAN_POINT ( 'NONE',  ( -93.52287095715006160, -29.50248528299804818, 1.056150453629040253 ) ) ;
#60030=VERTEX_POINT ( 'NONE', #2283 ) ;
#60031=CARTESIAN_POINT ( 'NONE',  ( -8.335131950130996614, 18.48905954037022781, 11.49999999999998934 ) ) ;
#60034=LINE ( 'NONE', #43801, #99469 ) ;
#60036=CARTESIAN_POINT ( 'NONE',  ( -95.22287095715005023, -23.47596703998600631, 11.44779298504227860 ) ) ;
#60039=CARTESIAN_POINT ( 'NONE',  ( -12.91570554291229023, -15.35452705144416896, -1.500000000000002220 ) ) ;
#60040=CARTESIAN_POINT ( 'NONE',  ( 5.126256225908648823, -20.47799061884807870, 11.49999999999999645 ) ) ;
#60041=CARTESIAN_POINT ( 'NONE',  ( -28.24657929368988718, -24.87968172495813590, 7.481726558560294116 ) ) ;
#60042=CARTESIAN_POINT ( 'NONE',  ( -70.55208003325599009, -24.15602025860895807, 10.28564288303535967 ) ) ;
#60043=CARTESIAN_POINT ( 'NONE',  ( 14.53198226072946220, 16.64418356588832992, -1.500000000000002220 ) ) ;
#60045=EDGE_CURVE ( 'NONE', #27205, #18719, #33720, .T. ) ;
#60046=CARTESIAN_POINT ( 'NONE',  ( -9.284664653622879626, 18.31210316397345395, -1.500000000000002220 ) ) ;
#60047=DIRECTION ( 'NONE',  ( 3.773278334444166432E-23, -1.000000000000000000, 0.000000000000000000 ) ) ;
#60048=EDGE_CURVE ( 'NONE', #82714, #98447, #64700, .T. ) ;
#60050=CARTESIAN_POINT ( 'NONE',  ( -53.52287095715006870, -23.48786465467241058, 11.44779295918255002 ) ) ;
#60052=CARTESIAN_POINT ( 'NONE',  ( -89.40841769935761363, -25.36026716165461892, 4.902505258696291612 ) ) ;
#60053=CARTESIAN_POINT ( 'NONE',  ( -29.58953762381673869, -23.39421443057875294, -1.443836134715248631 ) ) ;
#60056=LINE ( 'NONE', #90983, #48624 ) ;
#60058=CARTESIAN_POINT ( 'NONE',  ( -76.49748031141828619, -24.65952944569303895, 1.056160979905700570 ) ) ;
#60059=CARTESIAN_POINT ( 'NONE',  ( 11.80677006232881254, 16.86875346446678137, -1.500000000000002220 ) ) ;
#60060=CARTESIAN_POINT ( 'NONE',  ( -15.55086147716002110, 14.89234021980106881, 11.49999999999999645 ) ) ;
#60061=VERTEX_POINT ( 'NONE', #87505 ) ;
#60063=DIRECTION ( 'NONE',  ( 0.000000000000000000, 0.9999999999976377785, 2.173523156925979975E-06 ) ) ;
#60064=CARTESIAN_POINT ( 'NONE',  ( 20.23429811176546167, 9.490607074118958764, 11.49999999999998934 ) ) ;
#60065=CARTESIAN_POINT ( 'NONE',  ( -34.52287095715007581, -24.51387760970724017, 9.387446482453404073 ) ) ;
#60066=PLANE ( 'NONE',  #41622 ) ;
#60067=ORIENTED_EDGE ( 'NONE', *, *, #7325, .T. ) ;
#60068=CARTESIAN_POINT ( 'NONE',  ( -112.5228709571500616, -29.50250786944525672, 11.44777988621622988 ) ) ;
#60070=CARTESIAN_POINT ( 'NONE',  ( -49.52204948630863157, -23.48786465467241058, 11.44779295918254824 ) ) ;
#60072=CARTESIAN_POINT ( 'NONE',  ( -2.496121100066326814, 20.73550571027955769, -1.500000000000002220 ) ) ;
#60075=CARTESIAN_POINT ( 'NONE',  ( -98.62287095715007013, -23.72747288104442021, -1.053458166803661333 ) ) ;
#60079=CARTESIAN_POINT ( 'NONE',  ( -100.5838740427371789, -25.00182538069146787, 7.747789668545043362 ) ) ;
#60080=CARTESIAN_POINT ( 'NONE',  ( 19.72786461798894209, 7.474574171381012100, -1.500000000000002220 ) ) ;
#60082=CARTESIAN_POINT ( 'NONE',  ( -117.5893284022649965, -24.34968618360934656, 0.1864209137778901626 ) ) ;
#60083=CARTESIAN_POINT ( 'NONE',  ( -99.78066557477396259, -25.12215640787303528, 6.943018770401670814 ) ) ;
#60084=CARTESIAN_POINT ( 'NONE',  ( -9.857415191643349672, 19.42730305858377449, 11.49999999999998934 ) ) ;
#60088=CARTESIAN_POINT ( 'NONE',  ( 7.827691340095081607, 20.28360254610759839, -1.500000000000002220 ) ) ;
#60090=CARTESIAN_POINT ( 'NONE',  ( 9.404896790668452411, 20.21284700076377305, 11.49999999999999645 ) ) ;
#60091=ORIENTED_EDGE ( 'NONE', *, *, #72494, .F. ) ;
#60092=DIRECTION ( 'NONE',  ( -3.773278334453080206E-23, 0.9999999999976377785, 2.173523156925979975E-06 ) ) ;
#60094=B_SPLINE_CURVE_WITH_KNOTS ( 'NONE', 3,
 ( #91218, #75983, #52168, #6492, #20701, #52667 ),
 .UNSPECIFIED., .F., .F.,
 ( 4, 2, 4 ),
 ( 0.000000000000000000, 0.001380764517853253371, 0.002761529035706506742 ),
 .UNSPECIFIED. ) ;
#60100=B_SPLINE_CURVE_WITH_KNOTS ( 'NONE', 3,
 ( #75560, #60866, #59868, #76067 ),
 .UNSPECIFIED., .F., .F.,
 ( 4, 4 ),
 ( 0.8911363386465329661, 0.9001427699186484999 ),
 .UNSPECIFIED. ) ;
#60102=EDGE_CURVE ( 'NONE', #89509, #43699, #79134, .T. ) ;
#60103=CARTESIAN_POINT ( 'NONE',  ( -41.52287095715006870, -23.47596703998600631, 11.44779298504229281 ) ) ;
#60104=CARTESIAN_POINT ( 'NONE',  ( -69.62287095715005592, -24.64965695001468404, 8.947790433994184056 ) ) ;
#60106=CARTESIAN_POINT ( 'NONE',  ( -63.62287095715004881, -24.65952944569303895, 1.056160979905696129 ) ) ;
#60107=CARTESIAN_POINT ( 'NONE',  ( -8.550378450311910683, 17.38971893761031851, 11.49999999999998934 ) ) ;
#60108=CARTESIAN_POINT ( 'NONE',  ( -31.52287095715006870, -24.51387760970724372, 9.387446482453428942 ) ) ;
#60110=CARTESIAN_POINT ( 'NONE',  ( -16.98888496755095545, 9.415225082695979353, 11.49999999999999645 ) ) ;
#60111=CARTESIAN_POINT ( 'NONE',  ( -130.5728709571500588, -23.56000036390796737, 11.50200000000000244 ) ) ;
#60112=EDGE_CURVE ( 'NONE', #93818, #21767, #69437, .T. ) ;
#60116=CARTESIAN_POINT ( 'NONE',  ( -102.6228709571500559, -24.65952944569304606, 1.056160979905702124 ) ) ;
#60117=CARTESIAN_POINT ( 'NONE',  ( -64.52287095715006160, -29.50250243563736774, 8.947779886222145151 ) ) ;
#60118=CARTESIAN_POINT ( 'NONE',  ( 16.84789977498956404, 10.09486508543780481, -1.500000000000002220 ) ) ;
#60119=CARTESIAN_POINT ( 'NONE',  ( -46.57704074403396532, -24.65952944569304606, 1.056160979905696351 ) ) ;
#60120=EDGE_LOOP ( 'NONE', ( #93247, #32324, #7152, #10270 ) ) ;
#60121=CARTESIAN_POINT ( 'NONE',  ( 4.073501596442082651, -21.17334570714589859, -1.500000000000002220 ) ) ;
#60122=CARTESIAN_POINT ( 'NONE',  ( -33.66794373389784312, -23.48786465467240347, 11.44779295918255535 ) ) ;
#60123=DIRECTION ( 'NONE',  ( -3.773278334453080206E-23, 0.9999999999976377785, 2.173523156925979975E-06 ) ) ;
#60124=CARTESIAN_POINT ( 'NONE',  ( -62.58953762381672448, -24.64965694238406968, 8.947790433994660120 ) ) ;
#60126=CARTESIAN_POINT ( 'NONE',  ( -99.54260921963015107, -25.18439459044040873, 3.861216775032092929 ) ) ;
#60127=CARTESIAN_POINT ( 'NONE',  ( -9.967090755842360039, -20.75144515299163217, -1.500000000000002220 ) ) ;
#60129=ADVANCED_FACE ( 'NONE', ( #20971 ), #51444, .T. ) ;
#60132=CARTESIAN_POINT ( 'NONE',  ( -51.30795378556842223, -25.25249061358302782, 3.767456410489268936 ) ) ;
#60133=CARTESIAN_POINT ( 'NONE',  ( 19.96388892861992659, -2.714421270036905032, 11.49999999999999645 ) ) ;
#60136=B_SPLINE_CURVE_WITH_KNOTS ( 'NONE', 3,
 ( #86382, #38698, #69663, #54438, #16865, #93478 ),
 .UNSPECIFIED., .F., .F.,
 ( 4, 2, 4 ),
 ( 6.384118678612497773E-06, 0.001386860460828374768, 0.002767336802978137122 ),
 .UNSPECIFIED. ) ;
#60138=DIRECTION ( 'NONE',  ( -3.773278334453079618E-23, 0.9999999999976377785, 2.173523156925979552E-06 ) ) ;
#60139=CARTESIAN_POINT ( 'NONE',  ( -38.55620429048340014, -24.64898659630527789, 1.056161002820819039 ) ) ;
#60140=CARTESIAN_POINT ( 'NONE',  ( 15.68239283413728735, 12.23493734220040530, -1.500000000000002220 ) ) ;
#60141=ADVANCED_FACE ( 'NONE', ( #97605 ), #36711, .T. ) ;
#60143=CARTESIAN_POINT ( 'NONE',  ( 15.11087362536062173, -12.71848776332401521, -1.500000000000002220 ) ) ;
#60144=CARTESIAN_POINT ( 'NONE',  ( -126.5566010655604146, -23.48786465467241769, 11.44779295918253759 ) ) ;
#60148=CARTESIAN_POINT ( 'NONE',  ( -72.62287095715005592, -23.47596703998600631, 11.44779298504227860 ) ) ;
#60149=CARTESIAN_POINT ( 'NONE',  ( -37.52287095715006870, -29.50250243563736774, 8.947779886222148704 ) ) ;
#60150=CARTESIAN_POINT ( 'NONE',  ( -10.41657757243416604, 17.86655067824183618, 11.49999999999999645 ) ) ;
#60153=CARTESIAN_POINT ( 'NONE',  ( -79.55620429048339304, -23.47596703998600276, 11.44779298504227683 ) ) ;
#60154=CARTESIAN_POINT ( 'NONE',  ( -7.854035805165779927, 21.33931789143995417, 11.49999999999999645 ) ) ;
#60155=ORIENTED_EDGE ( 'NONE', *, *, #79480, .T. ) ;
#60156=DIRECTION ( 'NONE',  ( -3.773278334453079618E-23, 0.9999999999976377785, 2.173523156925979975E-06 ) ) ;
#60158=CARTESIAN_POINT ( 'NONE',  ( -8.513533612778267923, 18.29693335657625042, 11.49999999999998934 ) ) ;
#60160=FACE_OUTER_BOUND ( 'NONE', #62150, .T. ) ;
#60161=VERTEX_POINT ( 'NONE', #29587 ) ;
#60165=CARTESIAN_POINT ( 'NONE',  ( 0.7049041324096299022, -22.85584899170066109, 11.49999999999998934 ) ) ;
#60167=CARTESIAN_POINT ( 'NONE',  ( -19.30636564405121902, 9.640216152154000184, -1.500000000000002220 ) ) ;
#60168=CARTESIAN_POINT ( 'NONE',  ( -123.5570537027430333, -23.48783264082477373, -1.443836473390086361 ) ) ;
#60169=LINE ( 'NONE', #21076, #100284 ) ;
#60170=CARTESIAN_POINT ( 'NONE',  ( 3.584315319034878211, 22.25550262085195286, 11.49999999999999645 ) ) ;
#60172=CARTESIAN_POINT ( 'NONE',  ( -29.16972745157253399, -25.14850294581162515, 3.778578365308990161 ) ) ;
#60173=CARTESIAN_POINT ( 'NONE',  ( 16.16784302627978320, -14.93143893958281154, 11.49999999999998934 ) ) ;
#60175=CARTESIAN_POINT ( 'NONE',  ( -41.46538131673724337, -25.10925854964650128, 3.231378914883284992 ) ) ;
#60176=ADVANCED_FACE ( 'NONE', ( #83371 ), #35721, .T. ) ;
#60178=CARTESIAN_POINT ( 'NONE',  ( -118.6228709571500559, -24.66019654487200086, 8.947790411086117501 ) ) ;
#60179=CARTESIAN_POINT ( 'NONE',  ( -90.56379504561553517, -23.48786465467241769, 11.44779295918255180 ) ) ;
#60180=ORIENTED_EDGE ( 'NONE', *, *, #56785, .T. ) ;
#60183=ORIENTED_EDGE ( 'NONE', *, *, #84339, .T. ) ;
#60186=CARTESIAN_POINT ( 'NONE',  ( -57.64347623875748639, -23.96119346886880663, -0.6495511937832122440 ) ) ;
#60187=CARTESIAN_POINT ( 'NONE',  ( -2.125485521908593078, 20.27274140177646444, -1.500000000000002220 ) ) ;
#60188=ORIENTED_EDGE ( 'NONE', *, *, #16004, .T. ) ;
#60190=CARTESIAN_POINT ( 'NONE',  ( -115.6228709571500559, -23.47596703998600631, 11.44779298504227860 ) ) ;
#60191=DIRECTION ( 'NONE',  ( 0.000000000000000000, 2.173523156925980399E-06, -0.9999999999976378895 ) ) ;
#60192=CARTESIAN_POINT ( 'NONE',  ( -51.55620429048339304, -24.64965694238574656, 8.947790433994207149 ) ) ;
#60193=EDGE_LOOP ( 'NONE', ( #23576, #84795, #44722, #32332 ) ) ;
#60195=DIRECTION ( 'NONE',  ( 0.000000000000000000, -0.9999999999976377785, -2.173523156925979128E-06 ) ) ;
#60196=CARTESIAN_POINT ( 'NONE',  ( 19.16185898538474675, 8.078635803559651052, 11.49999999999998934 ) ) ;
#60199=DIRECTION ( 'NONE',  ( -1.000000000000000000, -3.773278334444166432E-23, -8.201307841325785021E-29 ) ) ;
#60207=CARTESIAN_POINT ( 'NONE',  ( -55.62287095715004881, -23.48783264082478084, -1.443836473390068820 ) ) ;
#60209=CARTESIAN_POINT ( 'NONE',  ( -10.67647856527443473, 19.39090429279614369, 11.49999999999999645 ) ) ;
#60210=ORIENTED_EDGE ( 'NONE', *, *, #40044, .T. ) ;
#60211=DIRECTION ( 'NONE',  ( 0.000000000000000000, 0.9999999999976377785, 2.173523156925979128E-06 ) ) ;
#60212=CARTESIAN_POINT ( 'NONE',  ( 17.19246737676917292, 14.74310579602587090, 11.49999999999998934 ) ) ;
#60213=EDGE_CURVE ( 'NONE', #91720, #29240, #83987, .T. ) ;
#60214=EDGE_CURVE ( 'NONE', #82905, #41074, #37985, .T. ) ;
#60216=CARTESIAN_POINT ( 'NONE',  ( -115.6239650023384797, -24.92592662359561473, 8.075495903017996469 ) ) ;
#60218=VECTOR ( 'NONE', #66627, 1000.000000000000114 ) ;
#60219=B_SPLINE_CURVE_WITH_KNOTS ( 'NONE', 3,
 ( #4638, #43206, #65564, #74146, #65065, #10750, #89369, #4140 ),
 .UNSPECIFIED., .F., .F.,
 ( 4, 2, 2, 4 ),
 ( -0.001240355328176664289, -0.0002398155169398015051, 0.0007607242942970612789, 0.002761803916770779257 ),
 .UNSPECIFIED. ) ;
#60224=CARTESIAN_POINT ( 'NONE',  ( -19.30929855918770954, 5.666966705251045511, -1.500000000000002220 ) ) ;
#60227=FACE_OUTER_BOUND ( 'NONE', #16241, .T. ) ;
#60228=CARTESIAN_POINT ( 'NONE',  ( -15.13915969582853549, -16.40262476207453801, -1.500000000000002220 ) ) ;
#60230=EDGE_CURVE ( 'NONE', #36357, #56116, #74289, .T. ) ;
#60232=ORIENTED_EDGE ( 'NONE', *, *, #10765, .F. ) ;
#60233=DIRECTION ( 'NONE',  ( -3.773278334453079030E-23, 0.9999999999976377785, 2.173523156925979128E-06 ) ) ;
#60234=DIRECTION ( 'NONE',  ( 3.773278334444167608E-23, -1.000000000000000000, 0.000000000000000000 ) ) ;
#60236=PLANE ( 'NONE',  #78931 ) ;
#60237=CARTESIAN_POINT ( 'NONE',  ( -73.62287095715007013, -24.66019654487199020, 8.947790411086131712 ) ) ;
#60238=CARTESIAN_POINT ( 'NONE',  ( 15.80261042061247068, 11.49252619723154112, -1.500000000000002220 ) ) ;
#60239=DIRECTION ( 'NONE',  ( -3.773278334453079618E-23, 0.9999999999976377785, 2.173523156925979975E-06 ) ) ;
#60240=CARTESIAN_POINT ( 'NONE',  ( 10.45947017991876926, -18.73710855793504848, -1.500000000000002220 ) ) ;
#60241=CARTESIAN_POINT ( 'NONE',  ( -25.97212670940007584, -24.57999732512023883, 2.712287346642571428 ) ) ;
#60242=CARTESIAN_POINT ( 'NONE',  ( -120.5228709571501184, -23.48783264082477373, -1.443836473390081698 ) ) ;
#60243=PLANE ( 'NONE',  #76551 ) ;
#60244=CARTESIAN_POINT ( 'NONE',  ( -15.20078144808659992, 16.97451310947862169, -1.500000000000002220 ) ) ;
#60246=VECTOR ( 'NONE', #79410, 1000.000000000000114 ) ;
#60249=CARTESIAN_POINT ( 'NONE',  ( -33.52287095715007581, -23.48783264083359512, -1.443836473376374441 ) ) ;
#60250=CARTESIAN_POINT ( 'NONE',  ( -11.44242300287478820, -16.35863574123370512, 11.49999999999999645 ) ) ;
#60252=CARTESIAN_POINT ( 'NONE',  ( -74.59647172187636954, -23.96169478059713498, 10.65365249895717881 ) ) ;
#60253=DIRECTION ( 'NONE',  ( 3.773278334444167608E-23, -1.000000000000000000, 0.000000000000000000 ) ) ;
#60255=PLANE ( 'NONE',  #86632 ) ;
#60256=CARTESIAN_POINT ( 'NONE',  ( -124.5228709571501042, -24.51283580621365132, 0.6167428607019898035 ) ) ;
#60257=EDGE_CURVE ( 'NONE', #66619, #79051, #92422, .T. ) ;
#60258=CARTESIAN_POINT ( 'NONE',  ( -11.39883337241029793, 18.50525654427185884, -1.500000000000002220 ) ) ;
#60259=DIRECTION ( 'NONE',  ( -3.773278334453079030E-23, 0.9999999999976377785, 2.173523156925979128E-06 ) ) ;
#60260=CARTESIAN_POINT ( 'NONE',  ( -0.9579564967699066846, 19.55851204243107233, -1.500000000000002220 ) ) ;
#60261=DIRECTION ( 'NONE',  ( -3.773278334453079030E-23, 0.9999999999976377785, 2.173523156925979128E-06 ) ) ;
#60264=ORIENTED_EDGE ( 'NONE', *, *, #44669, .T. ) ;
#60268=CARTESIAN_POINT ( 'NONE',  ( 16.11427877760282001, 12.65940972936023812, 11.49999999999999645 ) ) ;
#60269=CARTESIAN_POINT ( 'NONE',  ( -39.42646868310482944, -25.31266292137979690, 5.336263692767317934 ) ) ;
#60270=VECTOR ( 'NONE', #70977, 1000.000000000000114 ) ;
#60272=ORIENTED_EDGE ( 'NONE', *, *, #35260, .F. ) ;
#60273=CARTESIAN_POINT ( 'NONE',  ( -72.52287095715007581, -24.65952944569304606, 1.056160979905697239 ) ) ;
#60274=CARTESIAN_POINT ( 'NONE',  ( -40.16027052433451416, -25.18430879010554690, 3.329283022737130171 ) ) ;
#60276=CARTESIAN_POINT ( 'NONE',  ( -61.59189125704995860, -29.50249900881161835, 7.371157290072014590 ) ) ;
#60277=ORIENTED_EDGE ( 'NONE', *, *, #34567, .T. ) ;
#60279=B_SPLINE_CURVE_WITH_KNOTS ( 'NONE', 3,
 ( #62253, #61759, #85071, #23664 ),
 .UNSPECIFIED., .F., .F.,
 ( 4, 4 ),
 ( 0.000000000000000000, 0.0001000000000000167422 ),
 .UNSPECIFIED. ) ;
#60281=CARTESIAN_POINT ( 'NONE',  ( -17.29220519630379016, 15.29500218549028645, 11.49999999999999645 ) ) ;
#60282=CARTESIAN_POINT ( 'NONE',  ( -22.70586268970451371, -1.818501321912391999, -1.500000000000002220 ) ) ;
#60283=CARTESIAN_POINT ( 'NONE',  ( -70.32380231474228083, -25.12298712672050982, 7.101635559041870494 ) ) ;
#60284=CARTESIAN_POINT ( 'NONE',  ( -67.52287095715009002, -24.34917612406836440, 0.1852690917426552120 ) ) ;
#60288=CARTESIAN_POINT ( 'NONE',  ( -110.5116840983523900, -24.83618233451450763, 1.606449574219537935 ) ) ;
#60289=CARTESIAN_POINT ( 'NONE',  ( 13.84421170697429737, -16.98027460053469895, 11.49999999999998934 ) ) ;
#60290=DIRECTION ( 'NONE',  ( 0.000000000000000000, -2.173523156925980399E-06, 0.9999999999976378895 ) ) ;
#60291=CARTESIAN_POINT ( 'NONE',  ( -87.51095070751176763, -24.15620529776628445, 10.23563542870660292 ) ) ;
#60292=CARTESIAN_POINT ( 'NONE',  ( -41.31493931824280708, -25.31165118850823603, 4.672661947695956108 ) ) ;
#60293=CARTESIAN_POINT ( 'NONE',  ( -78.58482598963436772, -24.51314013834315375, 0.6176544820404143987 ) ) ;
#60294=CARTESIAN_POINT ( 'NONE',  ( -117.6228709571500559, -24.33832256526968862, 0.1851278514119943652 ) ) ;
#60295=CARTESIAN_POINT ( 'NONE',  ( -48.62287095715004881, -29.50248528299804818, 1.056150453629033370 ) ) ;
#60297=CARTESIAN_POINT ( 'NONE',  ( 17.75789855128238770, 10.12834119215567164, -1.500000000000002220 ) ) ;
#60299=ORIENTED_EDGE ( 'NONE', *, *, #73734, .T. ) ;
#60300=ORIENTED_EDGE ( 'NONE', *, *, #91912, .F. ) ;
#60302=CARTESIAN_POINT ( 'NONE',  ( -22.27228905017084060, 5.866681652885556986, -1.500000000000002220 ) ) ;
#60303=CARTESIAN_POINT ( 'NONE',  ( -35.52287095715008292, -24.15431212366874547, -0.2830839119320505692 ) ) ;
#60304=CARTESIAN_POINT ( 'NONE',  ( -19.33604739795523741, 5.927148246271303655, -1.500000000000002220 ) ) ;
#60306=CARTESIAN_POINT ( 'NONE',  ( -27.15357404441686384, -24.72305439599990251, 2.243760839632586546 ) ) ;
#60307=CARTESIAN_POINT ( 'NONE',  ( -101.5228709571500758, -23.47596703998600631, 11.44779298504228215 ) ) ;
#60308=CARTESIAN_POINT ( 'NONE',  ( -64.62287095715005592, -24.66019654487198665, 8.947790411086131712 ) ) ;
#60309=DIRECTION ( 'NONE',  ( -3.773278334453079030E-23, 0.9999999999976377785, 2.173523156925979128E-06 ) ) ;
#60310=CARTESIAN_POINT ( 'NONE',  ( 20.36625868517733196, 6.724766957447481097, 11.49999999999999645 ) ) ;
#60311=ORIENTED_EDGE ( 'NONE', *, *, #54743, .F. ) ;
#60313=CARTESIAN_POINT ( 'NONE',  ( -74.52287095715007581, -24.65952944569304606, 1.056160979905697239 ) ) ;
#60314=ORIENTED_EDGE ( 'NONE', *, *, #9563, .F. ) ;
#60315=CARTESIAN_POINT ( 'NONE',  ( -16.63904852704994042, -12.34428335884295969, -1.500000000000002220 ) ) ;
#60317=VERTEX_POINT ( 'NONE', #22457 ) ;
#60320=B_SPLINE_SURFACE_WITH_KNOTS ( 'NONE', 3, 3, ( 
 ( #99008, #37126, #52856, #68085 ),
 ( #92402, #62473, #53364, #31009 ),
 ( #38117, #61976, #69073, #93400 ),
 ( #22874, #30004, #99998, #83794 ),
 ( #45248, #30507, #39120, #84794 ),
 ( #15277, #22378, #68581, #60976 ),
 ( #46239, #92902, #84290, #77170 ) ),
 .UNSPECIFIED., .F., .F., .F.,
 ( 4, 3, 4 ),
 ( 4, 4 ),
 ( 0.3389563248807680451, 0.5103010155056330044, 0.6816457061304979081 ),
 ( 0.1860178884124073506, 0.2169648086611711268 ),
 .UNSPECIFIED. ) ;
#60321=CARTESIAN_POINT ( 'NONE',  ( -28.56161963849136498, -23.57732030158533476, -1.055554491438110309 ) ) ;
#60322=ORIENTED_EDGE ( 'NONE', *, *, #28443, .F. ) ;
#60325=ORIENTED_EDGE ( 'NONE', *, *, #70748, .F. ) ;
#60326=EDGE_CURVE ( 'NONE', #16463, #71288, #56452, .T. ) ;
#60328=CARTESIAN_POINT ( 'NONE',  ( 12.56776941831905070, -16.83212535568997126, -1.500000000000002220 ) ) ;
#60329=CARTESIAN_POINT ( 'NONE',  ( -19.44315311050126382, -10.23602577120861667, 11.49999999999999645 ) ) ;
#60331=CARTESIAN_POINT ( 'NONE',  ( -73.51158995227403636, -23.96169478059713143, 10.65365249895718236 ) ) ;
#60332=CARTESIAN_POINT ( 'NONE',  ( 20.50669422456317292, -9.396423750077818937, 11.49999999999998934 ) ) ;
#60334=CARTESIAN_POINT ( 'NONE',  ( -20.97355972163249049, 0.1317905507124840780, -1.500000000000002220 ) ) ;
#60335=CARTESIAN_POINT ( 'NONE',  ( -89.62287095715007013, -24.33832256527049864, 0.1851278514138624265 ) ) ;
#60336=EDGE_CURVE ( 'NONE', #43450, #100181, #17871, .T. ) ;
#60337=CARTESIAN_POINT ( 'NONE',  ( -89.40841769935767047, -25.26877885127129986, 5.947789088311301597 ) ) ;
#60338=FACE_OUTER_BOUND ( 'NONE', #90457, .T. ) ;
#60339=ORIENTED_EDGE ( 'NONE', *, *, #20821, .F. ) ;
#60342=VERTEX_POINT ( 'NONE', #49842 ) ;
#60344=CARTESIAN_POINT ( 'NONE',  ( -128.6228709571500701, -24.35013146730203815, 9.818937971375104823 ) ) ;
#60345=CARTESIAN_POINT ( 'NONE',  ( 8.792760106793807040, 19.66521392739144858, -1.500000000000002220 ) ) ;
#60347=ORIENTED_EDGE ( 'NONE', *, *, #75307, .T. ) ;
#60348=CARTESIAN_POINT ( 'NONE',  ( -19.14942259116913092, -8.910193081567555851, -1.500000000000002220 ) ) ;
#60349=LINE ( 'NONE', #91275, #38494 ) ;
#60351=CARTESIAN_POINT ( 'NONE',  ( -83.55852081072703186, -23.73791477778911840, 11.05961554403170588 ) ) ;
#60352=CARTESIAN_POINT ( 'NONE',  ( -79.52287095715006160, -23.48786465467241058, 11.44779295918254469 ) ) ;
#60354=CARTESIAN_POINT ( 'NONE',  ( 5.627179592841175193, 21.36305014179116668, -1.500000000000002220 ) ) ;
#60355=DIRECTION ( 'NONE',  ( -3.773278334453079618E-23, 0.9999999999976377785, 2.173523156925979975E-06 ) ) ;
#60356=EDGE_CURVE ( 'NONE', #60837, #83380, #48329, .T. ) ;
#60357=ORIENTED_EDGE ( 'NONE', *, *, #55166, .T. ) ;
#60358=CARTESIAN_POINT ( 'NONE',  ( -51.93149462243456327, -25.24860260566776660, 6.174051151396142245 ) ) ;
#60359=CARTESIAN_POINT ( 'NONE',  ( -79.62287095715005592, -23.47593901973091235, -1.443836447539004642 ) ) ;
#60360=CARTESIAN_POINT ( 'NONE',  ( -99.52287095715006160, -24.64965694238407323, 8.947790433994194714 ) ) ;
#60364=B_SPLINE_CURVE_WITH_KNOTS ( 'NONE', 3,
 ( #61397, #53780, #6090, #68004 ),
 .UNSPECIFIED., .F., .F.,
 ( 4, 4 ),
 ( 2.775557561562891043E-17, 9.999999999998898659E-05 ),
 .UNSPECIFIED. ) ;
#60365=CARTESIAN_POINT ( 'NONE',  ( -4.672984603565591755, -18.88948546680484242, 11.49999999999998934 ) ) ;
#60367=CARTESIAN_POINT ( 'NONE',  ( -10.59417575825165159, 18.57464501519095279, -1.500000000000002220 ) ) ;
#60369=B_SPLINE_CURVE_WITH_KNOTS ( 'NONE', 3,
 ( #60337, #14127, #47473, #78400 ),
 .UNSPECIFIED., .F., .F.,
 ( 4, 4 ),
 ( 0.000000000000000000, 0.0005192307692308412159 ),
 .UNSPECIFIED. ) ;
#60370=LINE ( 'NONE', #59861, #23626 ) ;
#60373=CARTESIAN_POINT ( 'NONE',  ( 4.697487806458584991, -22.17256498326293013, -1.500000000000002220 ) ) ;
#60374=VERTEX_POINT ( 'NONE', #80775 ) ;
#60376=CARTESIAN_POINT ( 'NONE',  ( -102.5895376238167387, -24.64965694238575011, 8.947790433994194714 ) ) ;
#60377=CARTESIAN_POINT ( 'NONE',  ( 12.93213199337649044, -14.99640713134888692, 11.49999999999999645 ) ) ;
#60379=CARTESIAN_POINT ( 'NONE',  ( -35.62287095715005592, -25.00158670708908915, 2.256160236439166855 ) ) ;
#60380=ORIENTED_EDGE ( 'NONE', *, *, #3975, .T. ) ;
#60382=B_SPLINE_CURVE_WITH_KNOTS ( 'NONE', 3,
 ( #34169, #80332, #81336, #40770, #25547, #97054 ),
 .UNSPECIFIED., .F., .F.,
 ( 4, 2, 4 ),
 ( 0.000000000000000000, 0.001380764517854768652, 0.002761529035709537304 ),
 .UNSPECIFIED. ) ;
#60383=DIRECTION ( 'NONE',  ( 0.000000000000000000, -0.9999999999976377785, -2.173523156925979975E-06 ) ) ;
#60384=CARTESIAN_POINT ( 'NONE',  ( 20.55956107658784404, -6.795330137259728787, 11.49999999999998934 ) ) ;
#60385=CARTESIAN_POINT ( 'NONE',  ( -49.59577668750772972, -25.27517929962447951, 3.074245939016678975 ) ) ;
#60386=CARTESIAN_POINT ( 'NONE',  ( 19.37663158793545293, -0.8356294931911363300, -1.500000000000002220 ) ) ;
#60387=CARTESIAN_POINT ( 'NONE',  ( -80.52287095715006160, -24.92604778743017846, 8.074972756849362554 ) ) ;
#60390=CARTESIAN_POINT ( 'NONE',  ( -7.013475202606065828, -18.52788797337992222, -1.500000000000002220 ) ) ;
#60391=VERTEX_POINT ( 'NONE', #16863 ) ;
#60392=CARTESIAN_POINT ( 'NONE',  ( 3.729398819442638846, -20.01364129133569136, 11.49999999999999645 ) ) ;
#60397=ORIENTED_EDGE ( 'NONE', *, *, #81178, .T. ) ;
#60398=DIRECTION ( 'NONE',  ( 1.000000000000000000, 3.773278334444166432E-23, 8.201307841325785021E-29 ) ) ;
#60399=CARTESIAN_POINT ( 'NONE',  ( -62.62287095715004881, -24.64898659630528854, 1.056161002820822592 ) ) ;
#60400=PLANE ( 'NONE',  #36981 ) ;
#60402=CARTESIAN_POINT ( 'NONE',  ( -51.27501529246699619, -25.17319112662202585, 6.792536120916223830 ) ) ;
#60403=CARTESIAN_POINT ( 'NONE',  ( -16.72505113720834657, 11.10480813184383742, 11.49999999999998934 ) ) ;
#60405=ORIENTED_EDGE ( 'NONE', *, *, #58665, .T. ) ;
#60406=CARTESIAN_POINT ( 'NONE',  ( -31.52287095715006160, -29.50247984919015209, -1.443849546365062242 ) ) ;
#60407=CARTESIAN_POINT ( 'NONE',  ( -22.55118551311790753, 3.560990644294375063, 11.49999999999999645 ) ) ;
#60408=CARTESIAN_POINT ( 'NONE',  ( -105.9228709571500531, -23.47593901973090524, -1.443836447538996870 ) ) ;
#60410=CARTESIAN_POINT ( 'NONE',  ( -115.6228709571500417, -23.48783264082478794, -1.443836473390058384 ) ) ;
#60411=DIRECTION ( 'NONE',  ( -3.773278334444166432E-23, 1.000000000000000000, 0.000000000000000000 ) ) ;
#60413=FACE_OUTER_BOUND ( 'NONE', #41117, .T. ) ;
#60414=CARTESIAN_POINT ( 'NONE',  ( -37.62287095715005592, -24.66019654487199020, 8.947790411086135265 ) ) ;
#60416=CARTESIAN_POINT ( 'NONE',  ( -19.47531982339030776, -5.969937916086089480, -1.500000000000002220 ) ) ;
#60418=CARTESIAN_POINT ( 'NONE',  ( 19.50756536182865020, -12.10693203178887423, 11.49999999999998934 ) ) ;
#60419=CARTESIAN_POINT ( 'NONE',  ( -32.52611253423770421, -24.65952944569304606, 1.056160979905696351 ) ) ;
#60420=ORIENTED_EDGE ( 'NONE', *, *, #5593, .T. ) ;
#60421=CARTESIAN_POINT ( 'NONE',  ( -108.6261691894128063, -24.35071581493544102, 9.817618358456016381 ) ) ;
#60422=CARTESIAN_POINT ( 'NONE',  ( -77.49792482936582871, -24.66019654487200441, 8.947790411086108620 ) ) ;
#60423=AXIS2_PLACEMENT_3D ( 'NONE', #30012, #13285, #20899 ) ;
#60424=CARTESIAN_POINT ( 'NONE',  ( -51.57778911984880210, -24.66019654487199730, 8.947790411086117501 ) ) ;
#60425=CARTESIAN_POINT ( 'NONE',  ( -7.839647760473957838, 19.78794240023834661, 11.49999999999999645 ) ) ;
#60426=ORIENTED_EDGE ( 'NONE', *, *, #81532, .F. ) ;
#60429=CARTESIAN_POINT ( 'NONE',  ( 13.39142644571787422, -17.71860720625715757, 11.49999999999998934 ) ) ;
#60430=CARTESIAN_POINT ( 'NONE',  ( -20.25002411749221665, -3.895867502427604379, 11.49999999999998934 ) ) ;
#60431=ORIENTED_EDGE ( 'NONE', *, *, #49631, .T. ) ;
#60433=ORIENTED_EDGE ( 'NONE', *, *, #76806, .F. ) ;
#60434=EDGE_CURVE ( 'NONE', #25965, #18516, #37794, .T. ) ;
#60435=FACE_OUTER_BOUND ( 'NONE', #17767, .T. ) ;
#60437=ORIENTED_EDGE ( 'NONE', *, *, #64947, .T. ) ;
#60438=EDGE_CURVE ( 'NONE', #64588, #38183, #94766, .T. ) ;
#60439=ORIENTED_EDGE ( 'NONE', *, *, #60526, .T. ) ;
#60441=LINE ( 'NONE', #79139, #38245 ) ;
#60442=CARTESIAN_POINT ( 'NONE',  ( -41.60044718131246100, -23.96169478059712432, 10.65365249895718591 ) ) ;
#60443=CARTESIAN_POINT ( 'NONE',  ( -56.62287095715005592, -29.50247984919015209, -1.443849546365056913 ) ) ;
#60444=CARTESIAN_POINT ( 'NONE',  ( -14.80784184970232431, -14.63167926507950689, -1.500000000000002220 ) ) ;
#60445=CARTESIAN_POINT ( 'NONE',  ( 11.26692973276593968, -18.67385317477220497, 11.49999999999999645 ) ) ;
#60446=EDGE_CURVE ( 'NONE', #38706, #80888, #47510, .T. ) ;
#60447=CARTESIAN_POINT ( 'NONE',  ( -50.79320621498229826, -25.03929677109420027, 7.533075084478241479 ) ) ;
#60449=CARTESIAN_POINT ( 'NONE',  ( 4.981011153104904388, 21.88276397462241363, 11.49999999999998934 ) ) ;
#60450=EDGE_CURVE ( 'NONE', #77746, #53293, #41727, .T. ) ;
#60451=CARTESIAN_POINT ( 'NONE',  ( -51.08807254026520184, -25.31296702852269576, 4.449946140181717524 ) ) ;
#60452=ORIENTED_EDGE ( 'NONE', *, *, #38598, .F. ) ;
#60453=CARTESIAN_POINT ( 'NONE',  ( 5.514125806255895004E-17, -29.50250786944496539, 11.44777975102276812 ) ) ;
#60456=EDGE_CURVE ( 'NONE', #91001, #100004, #39053, .T. ) ;
#60457=VERTEX_POINT ( 'NONE', #74646 ) ;
#60460=CARTESIAN_POINT ( 'NONE',  ( -95.52287095715006160, -29.50248528299804818, 1.056150453629042030 ) ) ;
#60461=ORIENTED_EDGE ( 'NONE', *, *, #90920, .F. ) ;
#60462=CARTESIAN_POINT ( 'NONE',  ( 13.34776491790984210, -16.67230741956907991, -1.500000000000002220 ) ) ;
#60463=VERTEX_POINT ( 'NONE', #65575 ) ;
#60464=CARTESIAN_POINT ( 'NONE',  ( -40.62287095715004170, -25.00182538069145011, 7.747789668545099317 ) ) ;
#60465=CARTESIAN_POINT ( 'NONE',  ( -20.94189920129180038, 1.864940847883316488, -1.500000000000002220 ) ) ;
#60466=DIRECTION ( 'NONE',  ( 0.000000000000000000, -2.173523156925979552E-06, 0.9999999999976378895 ) ) ;
#60468=LINE ( 'NONE', #29987, #57890 ) ;
#60469=CARTESIAN_POINT ( 'NONE',  ( 4.863445656156933694, -21.36585520573490626, -1.500000000000002220 ) ) ;
#60470=CARTESIAN_POINT ( 'NONE',  ( -39.52287095715005449, -24.51283580621365132, 0.6167428607019651565 ) ) ;
#60472=CARTESIAN_POINT ( 'NONE',  ( -58.62287095715004881, -24.64965695001468404, 8.947790433994185832 ) ) ;
#60473=AXIS2_PLACEMENT_3D ( 'NONE', #80275, #41733, #66080 ) ;
#60474=CARTESIAN_POINT ( 'NONE',  ( -84.51364942372109113, -23.96169478059713498, 10.65365249895717881 ) ) ;
#60475=B_SPLINE_CURVE_WITH_KNOTS ( 'NONE', 3,
 ( #68360, #5949, #13556, #36407, #59252, #83060, #83568, #67868, #5455, #28794, #98795, #76449, #91679, #29790, #52137, #74469, #52633, #21659 ),
 .UNSPECIFIED., .F., .F.,
 ( 4, 2, 2, 2, 2, 2, 2, 2, 4 ),
 ( 0.000000000000000000, 0.0001035810172459879051, 0.0002071620344919758102, 0.0004143240689839454405, 0.0008286481379678616076, 0.001035810172459820152, 0.001242972206951778588, 0.001450134241443737241, 0.001657296275935695676 ),
 .UNSPECIFIED. ) ;
#60477=CARTESIAN_POINT ( 'NONE',  ( -130.5728709571500588, -24.37907397113050934, 9.703205396196688426 ) ) ;
#60478=CARTESIAN_POINT ( 'NONE',  ( -0.008165308626489691315, -22.94429366319002028, 5.002395802403317049 ) ) ;
#60479=CARTESIAN_POINT ( 'NONE',  ( 15.78869406909177897, -14.30566568001193950, 11.49999999999998934 ) ) ;
#60480=CARTESIAN_POINT ( 'NONE',  ( -98.62355868264205583, -24.66019654487200086, 8.947790411086119278 ) ) ;
#60481=CARTESIAN_POINT ( 'NONE',  ( -54.55620429048339304, -23.47593901973091235, -1.443836447539009749 ) ) ;
#60484=CARTESIAN_POINT ( 'NONE',  ( -8.519796113377745783, 20.75715399588506926, -1.500000000000002220 ) ) ;
#60486=EDGE_LOOP ( 'NONE', ( #21271, #23485, #47555, #40336 ) ) ;
#60487=CARTESIAN_POINT ( 'NONE',  ( -72.52287095715010423, -23.48783264082476308, -1.443836473390092578 ) ) ;
#60488=CARTESIAN_POINT ( 'NONE',  ( 3.881049643139886207, -19.21785841795820104, 11.49999999999999645 ) ) ;
#60489=CARTESIAN_POINT ( 'NONE',  ( -108.5228709571500900, -24.33927499327855415, 9.819080762295804732 ) ) ;
#60490=CARTESIAN_POINT ( 'NONE',  ( -76.58953762381673869, -24.64965694238407679, 8.947790433994653014 ) ) ;
#60491=ORIENTED_EDGE ( 'NONE', *, *, #56157, .T. ) ;
#60492=CARTESIAN_POINT ( 'NONE',  ( -88.54555701694573600, -24.51419770103157703, 9.386484678747176957 ) ) ;
#60493=CARTESIAN_POINT ( 'NONE',  ( -31.62287095715005236, -29.50248528299804818, 1.056150453629029817 ) ) ;
#60494=CARTESIAN_POINT ( 'NONE',  ( -91.96387813629002039, -25.32379766982192848, 4.367815445636563432 ) ) ;
#60495=CARTESIAN_POINT ( 'NONE',  ( -108.6228709571500559, -29.50248528299804818, 1.056150453629043584 ) ) ;
#60496=B_SPLINE_CURVE_WITH_KNOTS ( 'NONE', 3,
 ( #61238, #92158, #4073, #30765, #816, #7925 ),
 .UNSPECIFIED., .F., .F.,
 ( 4, 2, 4 ),
 ( 6.384118695054804036E-06, 0.001386860460836599309, 0.002767336802978144061 ),
 .UNSPECIFIED. ) ;
#60498=CARTESIAN_POINT ( 'NONE',  ( -19.67082186522023690, -1.387426831159568108, -1.500000000000002220 ) ) ;
#60500=CARTESIAN_POINT ( 'NONE',  ( -120.6228709571500417, -29.50248789122583659, 2.256150453626215580 ) ) ;
#60502=ADVANCED_FACE ( 'NONE', ( #5141 ), #20693, .T. ) ;
#60506=VERTEX_POINT ( 'NONE', #81266 ) ;
#60507=CARTESIAN_POINT ( 'NONE',  ( -56.52287095715006870, -23.48786465467241058, 11.44779295918254824 ) ) ;
#60508=CARTESIAN_POINT ( 'NONE',  ( -67.62287095715005592, -24.65952944569304606, 1.056160979905697017 ) ) ;
#60511=CARTESIAN_POINT ( 'NONE',  ( -121.5562042904833930, -24.65952944569305316, 1.056160979905706565 ) ) ;
#60512=CARTESIAN_POINT ( 'NONE',  ( -31.24388727629348494, -24.86441894802673147, 8.247789967202360017 ) ) ;
#60514=CARTESIAN_POINT ( 'NONE',  ( -107.5967310269383574, -23.48783264082479505, -1.443836473390060826 ) ) ;
#60515=CARTESIAN_POINT ( 'NONE',  ( -3.050325703546597822, 19.74810961616558913, -1.500000000000002220 ) ) ;
#60517=DIRECTION ( 'NONE',  ( 3.773278334444167608E-23, -1.000000000000000000, 0.000000000000000000 ) ) ;
#60518=ORIENTED_EDGE ( 'NONE', *, *, #13386, .T. ) ;
#60520=CARTESIAN_POINT ( 'NONE',  ( -119.6241227149520228, -24.51314013834316086, 0.6176544820404245018 ) ) ;
#60521=CARTESIAN_POINT ( 'NONE',  ( -80.50429440537433834, -24.40133493613049964, 9.663955038902802386 ) ) ;
#60522=CARTESIAN_POINT ( 'NONE',  ( -81.52287095715010423, -23.48783264083388289, -1.443836473375922580 ) ) ;
#60523=CARTESIAN_POINT ( 'NONE',  ( -39.49835484170713329, -24.15543982623906416, -0.2315651400026678131 ) ) ;
#60524=CARTESIAN_POINT ( 'NONE',  ( -118.6228709571500559, -29.50250243563736774, 8.947779886222134493 ) ) ;
#60526=EDGE_CURVE ( 'NONE', #16871, #28343, #13705, .T. ) ;
#60532=CARTESIAN_POINT ( 'NONE',  ( -8.335131950130996614, 18.48905954037022781, -1.500000000000002220 ) ) ;
#60533=CARTESIAN_POINT ( 'NONE',  ( -68.94617219721770596, -25.27411024655319238, 6.009931644431809161 ) ) ;
#60538=FACE_OUTER_BOUND ( 'NONE', #93101, .T. ) ;
#60539=CARTESIAN_POINT ( 'NONE',  ( -62.52287095715006160, -23.47596703998600631, 11.44779298504228926 ) ) ;
#60540=CARTESIAN_POINT ( 'NONE',  ( -19.81368827760683260, -3.497637702615509880, -1.500000000000002220 ) ) ;
#60542=CARTESIAN_POINT ( 'NONE',  ( 8.294003578737715543, -19.35633765900385939, 11.49999999999999645 ) ) ;
#60543=CARTESIAN_POINT ( 'NONE',  ( -89.81226385320384509, -25.31959802671284265, 5.296208655838286816 ) ) ;
#60544=CARTESIAN_POINT ( 'NONE',  ( 7.643743511751816655, -20.74876368896106271, 11.49999999999998934 ) ) ;
#60545=B_SPLINE_CURVE_WITH_KNOTS ( 'NONE', 3,
 ( #99094, #60569, #91487, #67683 ),
 .UNSPECIFIED., .F., .F.,
 ( 4, 4 ),
 ( 0.000000000000000000, 1.000000000000000000 ),
 .UNSPECIFIED. ) ;
#60546=B_SPLINE_CURVE_WITH_KNOTS ( 'NONE', 3,
 ( #32023, #79196, #3100, #56889, #34035, #94423, #80205, #71101 ),
 .UNSPECIFIED., .F., .F.,
 ( 4, 2, 2, 4 ),
 ( 6.391158118970771556E-06, 0.002007136338672931355, 0.003007508928949909066, 0.004007881519226886777 ),
 .UNSPECIFIED. ) ;
#60547=CARTESIAN_POINT ( 'NONE',  ( -16.44861368136865920, 12.28130381464353782, 11.49999999999998934 ) ) ;
#60549=CARTESIAN_POINT ( 'NONE',  ( -114.6228709571500559, -24.64965695001469115, 8.947790433994176951 ) ) ;
#60550=ORIENTED_EDGE ( 'NONE', *, *, #81422, .T. ) ;
#60553=CARTESIAN_POINT ( 'NONE',  ( -83.22287095715005023, -23.47596703998600631, 11.44779298504227683 ) ) ;
#60555=ORIENTED_EDGE ( 'NONE', *, *, #3086, .T. ) ;
#60557=CARTESIAN_POINT ( 'NONE',  ( -118.6228709571500701, -24.50216790748100237, 0.6166512839513690336 ) ) ;
#60558=CARTESIAN_POINT ( 'NONE',  ( -98.62287095715005592, -29.50250243563736774, 8.947779886222138046 ) ) ;
#60559=CARTESIAN_POINT ( 'NONE',  ( -62.62287095715004881, -29.50247984919015209, -1.443849546365056913 ) ) ;
#60560=CARTESIAN_POINT ( 'NONE',  ( -9.109090448966927767, 18.51201596650851400, -1.500000000000002220 ) ) ;
#60561=CARTESIAN_POINT ( 'NONE',  ( -21.34238180412542718, 3.497892552127677135, 11.49999999999999645 ) ) ;
#60563=CARTESIAN_POINT ( 'NONE',  ( -46.62287095715004881, -29.50250786944525672, 11.44777988621624054 ) ) ;
#60565=CARTESIAN_POINT ( 'NONE',  ( -0.4079105510268487000, 22.33655531192813370, -1.500000000000002220 ) ) ;
#60566=CARTESIAN_POINT ( 'NONE',  ( -80.48900664166535535, -25.27875090823107485, 7.101635220485683853 ) ) ;
#60567=DIRECTION ( 'NONE',  ( -3.773278334444167608E-23, 1.000000000000000000, 0.000000000000000000 ) ) ;
#60568=EDGE_LOOP ( 'NONE', ( #47365, #16832, #99445, #36461 ) ) ;
#60569=CARTESIAN_POINT ( 'NONE',  ( -43.55620429048339304, -23.47593901973091235, -1.443836447539011525 ) ) ;
#60570=CARTESIAN_POINT ( 'NONE',  ( -49.57748681740810071, -24.66019654487198665, 8.947790411086131712 ) ) ;
#60571=ADVANCED_FACE ( 'NONE', ( #46592 ), #74165, .T. ) ;
#60572=CARTESIAN_POINT ( 'NONE',  ( 18.75483278694074940, -9.228467059531109129, 11.49999999999998934 ) ) ;
#60575=CARTESIAN_POINT ( 'NONE',  ( -86.58558031640687602, -24.51314013834315375, 0.6176544820404177294 ) ) ;
#60578=VECTOR ( 'NONE', #18667, 1000.000000000000114 ) ;
#60579=CARTESIAN_POINT ( 'NONE',  ( -109.6292179679340251, -23.96169478059713853, 10.65365249895717703 ) ) ;
#60580=CARTESIAN_POINT ( 'NONE',  ( 1.943494986365726485, -21.02143711168614004, -1.500000000000002220 ) ) ;
#60581=EDGE_LOOP ( 'NONE', ( #26626, #85834, #62827, #98482 ) ) ;
#60582=CARTESIAN_POINT ( 'NONE',  ( -117.5579596701613951, -23.48783264082477729, -1.443836473390081254 ) ) ;
#60583=PLANE ( 'NONE',  #28811 ) ;
#60584=CARTESIAN_POINT ( 'NONE',  ( 21.63681353182189682, 2.665401433100548889, 11.49999999999998934 ) ) ;
#60585=CARTESIAN_POINT ( 'NONE',  ( -120.6293623597568825, -23.48786465467241769, 11.44779295918253936 ) ) ;
#60589=CARTESIAN_POINT ( 'NONE',  ( 1.329761939549756855, 21.69843865049760367, -1.500000000000002220 ) ) ;
#60590=CARTESIAN_POINT ( 'NONE',  ( -71.44479781437794941, -25.24674145135648828, 5.279211752121547363 ) ) ;
#60591=CARTESIAN_POINT ( 'NONE',  ( -19.39139147909919458, -11.06001032434818576, 11.49999999999999645 ) ) ;
#60593=ADVANCED_FACE ( 'NONE', ( #40479 ), #54214, .F. ) ;
#60596=CARTESIAN_POINT ( 'NONE',  ( -68.58953762381672448, -24.65952944569304250, 1.056160979905694131 ) ) ;
#60597=ORIENTED_EDGE ( 'NONE', *, *, #5582, .T. ) ;
#60598=EDGE_LOOP ( 'NONE', ( #28458, #40178, #86807, #83725 ) ) ;
#60599=VERTEX_POINT ( 'NONE', #32357 ) ;
#60600=CARTESIAN_POINT ( 'NONE',  ( -85.55620429048337883, -23.48786465467241058, 11.44779295918254292 ) ) ;
#60601=CARTESIAN_POINT ( 'NONE',  ( 19.38521227897113874, -8.589346653930519437, -1.500000000000002220 ) ) ;
#60606=CARTESIAN_POINT ( 'NONE',  ( -18.68205546197936684, -5.105407162728520021, 11.49999999999998934 ) ) ;
#60609=CARTESIAN_POINT ( 'NONE',  ( 15.33136405852079243, -11.96835230219363311, 11.49999999999999645 ) ) ;
#60610=CARTESIAN_POINT ( 'NONE',  ( -115.5228709571500616, -24.83620972994592435, 8.398175272781369216 ) ) ;
#60613=CARTESIAN_POINT ( 'NONE',  ( -53.52287095715005449, -24.66019654487198665, 8.947790411086121054 ) ) ;
#60615=CARTESIAN_POINT ( 'NONE',  ( -65.22287095715006444, -23.47596703998600631, 11.44779298504227860 ) ) ;
#60616=CARTESIAN_POINT ( 'NONE',  ( -120.9228709571500531, -23.47596703998600276, 11.44779298504227683 ) ) ;
#60617=ADVANCED_FACE ( 'NONE', ( #61822 ), #71432, .F. ) ;
#60618=CARTESIAN_POINT ( 'NONE',  ( 2.166912399371504705, 19.51343182558466793, -1.500000000000002220 ) ) ;
#60622=CARTESIAN_POINT ( 'NONE',  ( 16.61904782137575154, -13.72857183568914685, 11.49999999999998934 ) ) ;
#60623=CARTESIAN_POINT ( 'NONE',  ( -33.61929772658547222, -23.48786465467240347, 11.44779295918255535 ) ) ;
#60624=CARTESIAN_POINT ( 'NONE',  ( -123.5562042904833788, -23.48786465467241769, 11.44779295918253403 ) ) ;
#60625=CARTESIAN_POINT ( 'NONE',  ( -50.52287095715006160, -24.51163499207180152, 0.6490370598555512682 ) ) ;
#60626=CARTESIAN_POINT ( 'NONE',  ( -99.99551102217851906, -25.27473239134466354, 3.374614203793048439 ) ) ;
#60627=CARTESIAN_POINT ( 'NONE',  ( 1.550618966079767347, 22.99078241098900932, -1.500000000000002220 ) ) ;
#60628=ADVANCED_FACE ( 'NONE', ( #55717 ), #7515, .F. ) ;
#60630=CARTESIAN_POINT ( 'NONE',  ( -74.62287095715005592, -23.47596703998600631, 11.44779298504227860 ) ) ;
#60632=CARTESIAN_POINT ( 'NONE',  ( 20.11291949428234105, -1.170665973999911902, 11.49999999999999645 ) ) ;
#60633=CARTESIAN_POINT ( 'NONE',  ( -108.9559085688801616, -25.28814349977695386, 4.125625889878640429 ) ) ;
#60634=CARTESIAN_POINT ( 'NONE',  ( -32.66840245258526920, -23.48786465467240347, 11.44779295918255535 ) ) ;
#60635=CARTESIAN_POINT ( 'NONE',  ( -104.5895376238167245, -24.65952944569304606, 1.056160979905699238 ) ) ;
#60637=CARTESIAN_POINT ( 'NONE',  ( -110.3698707892751401, -25.18425582861542367, 3.294862445368111459 ) ) ;
#60638=CARTESIAN_POINT ( 'NONE',  ( -0.2410636032128395945, 19.88167143085883737, 11.49999999999998934 ) ) ;
#60640=CARTESIAN_POINT ( 'NONE',  ( -1.996473883165060581, 19.68112600131995293, -1.500000000000002220 ) ) ;
#60642=CARTESIAN_POINT ( 'NONE',  ( -125.6228709571500559, -24.99156045073393173, 7.747789690856161648 ) ) ;
#60644=CARTESIAN_POINT ( 'NONE',  ( 16.58470376584361361, 12.37529123428901556, 11.49999999999999645 ) ) ;
#60646=B_SPLINE_CURVE_WITH_KNOTS ( 'NONE', 3,
 ( #32039, #39648, #54386, #46771 ),
 .UNSPECIFIED., .F., .F.,
 ( 4, 4 ),
 ( 0.000000000000000000, 9.999999999997510880E-05 ),
 .UNSPECIFIED. ) ;
#60649=CARTESIAN_POINT ( 'NONE',  ( -50.34100630499489881, -25.25138672863312550, 5.198616883439322933 ) ) ;
#60650=CARTESIAN_POINT ( 'NONE',  ( 18.51665531608540860, 13.21585733361752801, 11.49999999999999645 ) ) ;
#60651=ORIENTED_EDGE ( 'NONE', *, *, #72702, .F. ) ;
#60652=CARTESIAN_POINT ( 'NONE',  ( -60.62287095715003460, -24.83602698348160231, 1.605859176311265513 ) ) ;
#60654=CARTESIAN_POINT ( 'NONE',  ( 15.40757771627215256, 13.04930689719894765, 11.49999999999998934 ) ) ;
#60655=CARTESIAN_POINT ( 'NONE',  ( -63.61013885863124528, -23.48783264082475952, -1.443836473390093245 ) ) ;
#60656=CARTESIAN_POINT ( 'NONE',  ( -41.42938027069750007, -25.29269197957483328, 4.439299310465838033 ) ) ;
#60657=EDGE_CURVE ( 'NONE', #53455, #16362, #73045, .T. ) ;
#60661=CARTESIAN_POINT ( 'NONE',  ( 22.59171682324826236, -3.780823453261925593, 11.49999999999998934 ) ) ;
#60662=DIRECTION ( 'NONE',  ( 0.000000000000000000, 0.9999999999976377785, 2.173523156925979128E-06 ) ) ;
#60663=CARTESIAN_POINT ( 'NONE',  ( -13.25059585359799108, -17.08168364658555305, -1.500000000000002220 ) ) ;
#60664=LINE ( 'NONE', #98701, #73914 ) ;
#60666=CARTESIAN_POINT ( 'NONE',  ( 3.889286922045745776, 20.52237432693057073, 11.49999999999999645 ) ) ;
#60667=ORIENTED_EDGE ( 'NONE', *, *, #63672, .T. ) ;
#60669=CARTESIAN_POINT ( 'NONE',  ( 17.71009474140864981, 13.04663522181963309, -1.500000000000002220 ) ) ;
#60670=AXIS2_PLACEMENT_3D ( 'NONE', #78079, #79595, #24309 ) ;
#60671=CARTESIAN_POINT ( 'NONE',  ( -105.5081692944722818, -24.92592662359561473, 8.075495903018000021 ) ) ;
#60672=CARTESIAN_POINT ( 'NONE',  ( -28.57615893954310238, -25.21724918667983673, 7.256891368531773523 ) ) ;
#60673=EDGE_LOOP ( 'NONE', ( #59421, #65350, #11687, #34475 ) ) ;
#60679=ORIENTED_EDGE ( 'NONE', *, *, #55514, .F. ) ;
#60682=CARTESIAN_POINT ( 'NONE',  ( -101.5937515207030657, -25.27404774504482887, 3.495447232644239399 ) ) ;
#60684=CARTESIAN_POINT ( 'NONE',  ( 15.88337727998148985, 12.78846505907953279, -1.500000000000002220 ) ) ;
#60685=AXIS2_PLACEMENT_3D ( 'NONE', #57319, #34958, #33957 ) ;
#60688=CARTESIAN_POINT ( 'NONE',  ( -30.60515864328932878, -24.57438384523503316, 0.5319095616429411200 ) ) ;
#60691=ORIENTED_EDGE ( 'NONE', *, *, #13208, .T. ) ;
#60693=CARTESIAN_POINT ( 'NONE',  ( -29.31102972132424966, -24.63645865963270865, 7.337444170384009645 ) ) ;
#60694=EDGE_CURVE ( 'NONE', #82898, #32935, #8860, .T. ) ;
#60695=CARTESIAN_POINT ( 'NONE',  ( 20.70993026999094511, 1.908435391604796028, -1.500000000000002220 ) ) ;
#60697=ORIENTED_EDGE ( 'NONE', *, *, #70209, .T. ) ;
#60698=CARTESIAN_POINT ( 'NONE',  ( -42.52287095715006160, -23.96177878511308279, 10.65340807706331283 ) ) ;
#60701=VERTEX_POINT ( 'NONE', #49104 ) ;
#60703=FACE_OUTER_BOUND ( 'NONE', #54925, .T. ) ;
#60704=CARTESIAN_POINT ( 'NONE',  ( -92.62287095715008434, -24.51387760970724017, 9.387446482453416507 ) ) ;
#60705=CARTESIAN_POINT ( 'NONE',  ( -116.6623382465025145, -25.28334050553294787, 4.245309122437062932 ) ) ;
#60706=CARTESIAN_POINT ( 'NONE',  ( -100.4979344782931037, -25.03152448927857066, 7.562057945188089825 ) ) ;
#60707=B_SPLINE_CURVE_WITH_KNOTS ( 'NONE', 3,
 ( #51078, #74891, #27241, #28735 ),
 .UNSPECIFIED., .F., .F.,
 ( 4, 4 ),
 ( 0.000000000000000000, 1.000000000000000000 ),
 .UNSPECIFIED. ) ;
#60708=CARTESIAN_POINT ( 'NONE',  ( -108.9572543305703363, -25.28095782085471299, 4.080816019651302362 ) ) ;
#60710=CARTESIAN_POINT ( 'NONE',  ( -13.28819421967561532, -17.68372732473523001, 11.49999999999999645 ) ) ;
#60711=ORIENTED_EDGE ( 'NONE', *, *, #6706, .F. ) ;
#60712=EDGE_CURVE ( 'NONE', #6687, #56269, #98351, .T. ) ;
#60713=CARTESIAN_POINT ( 'NONE',  ( -105.5895376238167387, -23.47596703998600631, 11.44779298504227683 ) ) ;
#60714=CARTESIAN_POINT ( 'NONE',  ( -22.62345309801473547, -0.4825844212548152656, -1.500000000000002220 ) ) ;
#60716=CARTESIAN_POINT ( 'NONE',  ( -77.52287095715006160, -24.66019654487200086, 8.947790411086113949 ) ) ;
#60718=ORIENTED_EDGE ( 'NONE', *, *, #98973, .F. ) ;
#60721=CARTESIAN_POINT ( 'NONE',  ( -19.48533387766964964, -5.011242947278518045, 11.49999999999998934 ) ) ;
#60722=B_SPLINE_SURFACE_WITH_KNOTS ( 'NONE', 3, 3, ( 
 ( #37995, #32890, #33884, #17154 ),
 ( #48120, #63863, #79554, #1946 ),
 ( #25264, #94776, #80055, #88178 ),
 ( #72455, #79050, #63358, #18156 ),
 ( #48628, #96284, #33375, #55740 ),
 ( #18646, #64363, #16649, #34387 ),
 ( #56243, #87168, #56743, #87674 ) ),
 .UNSPECIFIED., .F., .F., .F.,
 ( 4, 3, 4 ),
 ( 4, 4 ),
 ( 0.0004766839783845008469, 0.1029713700210910104, 0.2054660560637975308 ),
 ( 0.1595345801196773328, 0.1606209136378454749 ),
 .UNSPECIFIED. ) ;
#60726=CARTESIAN_POINT ( 'NONE',  ( -1.228339276683141579, -22.28195500894762660, -1.500000000000002220 ) ) ;
#60727=ORIENTED_EDGE ( 'NONE', *, *, #78327, .F. ) ;
#60729=CARTESIAN_POINT ( 'NONE',  ( -101.3540785649959304, -25.25341200507040540, 6.680569176468658554 ) ) ;
#60730=CARTESIAN_POINT ( 'NONE',  ( -81.78154518342495294, -25.18542598755805884, 6.709299554139687594 ) ) ;
#60732=CARTESIAN_POINT ( 'NONE',  ( -47.55620429048338593, -24.64898659630528499, 1.056161002820819261 ) ) ;
#60734=CARTESIAN_POINT ( 'NONE',  ( 18.95637782189878706, 4.751392969308117387, 11.49999999999998934 ) ) ;
#60735=CARTESIAN_POINT ( 'NONE',  ( -65.62287095715005592, -24.99156045073393173, 7.747789690856161648 ) ) ;
#60736=CARTESIAN_POINT ( 'NONE',  ( -13.16228656746626591, 16.97819584282690286, -1.500000000000002220 ) ) ;
#60738=CARTESIAN_POINT ( 'NONE',  ( -117.5228709571500758, -29.50248528299804818, 1.056150453629045360 ) ) ;
#60740=CARTESIAN_POINT ( 'NONE',  ( 22.28265747778879202, 5.072132558558076099, -1.500000000000002220 ) ) ;
#60742=ADVANCED_FACE ( 'NONE', ( #80532 ), #72933, .F. ) ;
#60744=CARTESIAN_POINT ( 'NONE',  ( -106.5198638994752542, -23.73791477778912551, 11.05961554403169700 ) ) ;
#60745=FACE_OUTER_BOUND ( 'NONE', #57919, .T. ) ;
#60746=CARTESIAN_POINT ( 'NONE',  ( -17.52048005523606022, -9.576713672051738513, 11.49999999999999645 ) ) ;
#60748=CARTESIAN_POINT ( 'NONE',  ( -123.6228709571500559, -24.64898659630368627, 1.056161002820833028 ) ) ;
#60749=CARTESIAN_POINT ( 'NONE',  ( -43.92287095715007439, -23.47593901973090524, -1.443836447538998424 ) ) ;
#60750=ORIENTED_EDGE ( 'NONE', *, *, #47260, .T. ) ;
#60751=CARTESIAN_POINT ( 'NONE',  ( -27.51805182407180794, -24.60240642400831135, 1.634233119128260636 ) ) ;
#60754=CARTESIAN_POINT ( 'NONE',  ( -19.25911440464646063, 10.06369110047026538, -1.500000000000002220 ) ) ;
#60755=CARTESIAN_POINT ( 'NONE',  ( -55.62287095715004170, -29.50249982740957577, 7.747779886224967605 ) ) ;
#60756=CARTESIAN_POINT ( 'NONE',  ( -15.04504930077994196, -12.58455232801425794, -1.500000000000002220 ) ) ;
#60757=DIRECTION ( 'NONE',  ( 0.000000000000000000, 2.173523156925980399E-06, -0.9999999999976378895 ) ) ;
#60762=CARTESIAN_POINT ( 'NONE',  ( -18.81443736134900035, 8.205417114561466718, 11.49999999999999645 ) ) ;
#60764=LINE ( 'NONE', #6465, #98307 ) ;
#60765=EDGE_CURVE ( 'NONE', #26090, #86743, #20890, .T. ) ;
#60766=ORIENTED_EDGE ( 'NONE', *, *, #10044, .T. ) ;
#60767=CARTESIAN_POINT ( 'NONE',  ( -110.0171095414734737, -25.30123833581429338, 5.384701099344828101 ) ) ;
#60768=CARTESIAN_POINT ( 'NONE',  ( -40.42371425561744047, -25.18430871546082628, 3.294940290805283389 ) ) ;
#60771=B_SPLINE_CURVE_WITH_KNOTS ( 'NONE', 3,
 ( #13375, #91499, #38213, #45348, #45840, #44354 ),
 .UNSPECIFIED., .F., .F.,
 ( 4, 2, 4 ),
 ( 0.000000000000000000, 0.001380901958385395700, 0.002761803916770791401 ),
 .UNSPECIFIED. ) ;
#60772=DIRECTION ( 'NONE',  ( 0.000000000000000000, -2.173523156925980399E-06, 0.9999999999976378895 ) ) ;
#60773=CARTESIAN_POINT ( 'NONE',  ( -99.52287095715006160, -23.48786465467241769, 11.44779295918254114 ) ) ;
#60776=EDGE_CURVE ( 'NONE', #50270, #23352, #58698, .T. ) ;
#60777=CARTESIAN_POINT ( 'NONE',  ( 5.194767643164344584, 22.50260600399833422, 11.49999999999999645 ) ) ;
#60778=CARTESIAN_POINT ( 'NONE',  ( 22.20583189720066741, -5.198064566299082756, -1.500000000000002220 ) ) ;
#60779=CARTESIAN_POINT ( 'NONE',  ( -110.5150696451292021, -24.40133493613049609, 9.663955038902800609 ) ) ;
#60780=CARTESIAN_POINT ( 'NONE',  ( -75.52287095715013265, -24.82576562948882071, 8.398263436605672538 ) ) ;
#60781=CARTESIAN_POINT ( 'NONE',  ( -123.5228709571500190, -24.51283580621364777, 0.6167428607019826980 ) ) ;
#60783=B_SPLINE_CURVE_WITH_KNOTS ( 'NONE', 3,
 ( #50249, #96415, #26901, #66981 ),
 .UNSPECIFIED., .F., .F.,
 ( 4, 4 ),
 ( 0.000000000000000000, 0.0001000000000000028644 ),
 .UNSPECIFIED. ) ;
#60785=CARTESIAN_POINT ( 'NONE',  ( -62.52287095715006160, -29.50248528299804818, 1.056150453629034924 ) ) ;
#60786=CARTESIAN_POINT ( 'NONE',  ( -110.5193718685209774, -23.85016227208580020, -0.8807180028928306426 ) ) ;
#60787=CARTESIAN_POINT ( 'NONE',  ( -19.33260374144687077, -10.33727041909969380, -1.500000000000002220 ) ) ;
#60788=CARTESIAN_POINT ( 'NONE',  ( -69.52210420424350446, -23.48786465467240347, 11.44779295918255002 ) ) ;
#60789=DIRECTION ( 'NONE',  ( -3.773278334453079030E-23, 0.9999999999976377785, 2.173523156925979128E-06 ) ) ;
#60791=CARTESIAN_POINT ( 'NONE',  ( -78.50466238525980600, -24.34968618360933945, 0.1864209137778830849 ) ) ;
#60792=CARTESIAN_POINT ( 'NONE',  ( -112.5228709571500616, -24.66019654487200441, 8.947790411086108620 ) ) ;
#60793=CARTESIAN_POINT ( 'NONE',  ( -76.52287095715011844, -23.48783264082477373, -1.443836473390087694 ) ) ;
#60795=CARTESIAN_POINT ( 'NONE',  ( 7.241121213506172438, 19.11196469071355963, -1.500000000000002220 ) ) ;
#60798=ORIENTED_EDGE ( 'NONE', *, *, #31008, .F. ) ;
#60800=EDGE_CURVE ( 'NONE', #46021, #17843, #86322, .T. ) ;
#60801=CARTESIAN_POINT ( 'NONE',  ( 19.44587849558928738, -12.39355811350142922, 11.49999999999998934 ) ) ;
#60803=CARTESIAN_POINT ( 'NONE',  ( 10.87751022112437482, 17.06716278085755079, -1.500000000000002220 ) ) ;
#60805=CARTESIAN_POINT ( 'NONE',  ( -48.52287095715006160, -24.64965694238574656, 8.947790433994203596 ) ) ;
#60807=CARTESIAN_POINT ( 'NONE',  ( -28.52287095715007226, -24.17764966940397287, 9.819270424401523201 ) ) ;
#60808=CARTESIAN_POINT ( 'NONE',  ( -99.56068028760604705, -23.48786465467241413, 11.44779295918254469 ) ) ;
#60809=CARTESIAN_POINT ( 'NONE',  ( 21.36505145794347982, 1.902718533054148509, 11.49999999999999645 ) ) ;
#60810=ORIENTED_EDGE ( 'NONE', *, *, #77825, .F. ) ;
#60811=CARTESIAN_POINT ( 'NONE',  ( -128.6228709571500133, -23.72747288104441665, -1.053458166803660001 ) ) ;
#60813=VERTEX_POINT ( 'NONE', #96264 ) ;
#60814=CARTESIAN_POINT ( 'NONE',  ( -14.56105648253378781, -14.73650127990469016, -1.500000000000002220 ) ) ;
#60816=EDGE_CURVE ( 'NONE', #81403, #88020, #7601, .T. ) ;
#60817=CARTESIAN_POINT ( 'NONE',  ( -80.52287095715007581, -23.48783264082477018, -1.443836473390091246 ) ) ;
#60819=B_SPLINE_CURVE_WITH_KNOTS ( 'NONE', 3,
 ( #21115, #14505, #20622, #98239, #44475, #37363, #90145, #74419, #76395, #5899, #6897, #51090, #52580, #67822, #60705, #61209, #74902, #36858 ),
 .UNSPECIFIED., .F., .F.,
 ( 4, 2, 2, 2, 2, 2, 2, 2, 4 ),
 ( 0.000000000000000000, 0.0005889166363242080444, 0.001177833272648416089, 0.001766749908972623266, 0.002355666545296830443, 0.002944583181621037403, 0.003533499817945244363, 0.004122416454269450456, 0.004711333090593654814 ),
 .UNSPECIFIED. ) ;
#60821=CARTESIAN_POINT ( 'NONE',  ( -28.62375884954849425, -24.50672967435375682, 1.056161677404372501 ) ) ;
#60822=ORIENTED_EDGE ( 'NONE', *, *, #30630, .T. ) ;
#60824=VERTEX_POINT ( 'NONE', #88156 ) ;
#60825=CARTESIAN_POINT ( 'NONE',  ( -16.59477544326466969, -14.39948450415919723, 11.49999999999999645 ) ) ;
#60828=CARTESIAN_POINT ( 'NONE',  ( -37.56099278926783569, -23.73791477778911130, 11.05961554403171299 ) ) ;
#60829=CARTESIAN_POINT ( 'NONE',  ( 6.936750662203477802, 21.44973376661030429, 11.49999999999998934 ) ) ;
#60831=CARTESIAN_POINT ( 'NONE',  ( 10.18035917307295435, 18.35650967997132099, -1.500000000000002220 ) ) ;
#60833=CARTESIAN_POINT ( 'NONE',  ( -108.9605944373618343, -25.29717339419269706, 4.328833245316407563 ) ) ;
#60835=ORIENTED_EDGE ( 'NONE', *, *, #76328, .F. ) ;
#60836=EDGE_CURVE ( 'NONE', #84257, #19500, #29348, .T. ) ;
#60837=VERTEX_POINT ( 'NONE', #21609 ) ;
#60838=VERTEX_POINT ( 'NONE', #30227 ) ;
#60839=CARTESIAN_POINT ( 'NONE',  ( -66.54011281632980968, -24.51314013834316441, 0.6176544820404136216 ) ) ;
#60840=CARTESIAN_POINT ( 'NONE',  ( 16.61460563260716583, 13.71664681387569118, -1.500000000000002220 ) ) ;
#60842=ORIENTED_EDGE ( 'NONE', *, *, #53502, .T. ) ;
#60843=CARTESIAN_POINT ( 'NONE',  ( 6.686094007546604878, -20.02240253118446844, -1.500000000000002220 ) ) ;
#60846=CARTESIAN_POINT ( 'NONE',  ( -64.52287095715006160, -23.48783264082476308, -1.443836473390094355 ) ) ;
#60847=PLANE ( 'NONE',  #96065 ) ;
#60849=CARTESIAN_POINT ( 'NONE',  ( -14.73459587841175633, -16.56598928932902837, -1.500000000000002220 ) ) ;
#60850=CARTESIAN_POINT ( 'NONE',  ( -71.49518700469006660, -24.65952944569304961, 1.056160979905700570 ) ) ;
#60852=CARTESIAN_POINT ( 'NONE',  ( -51.92928322226379123, -25.24860240139651424, 6.080069520644998171 ) ) ;
#60853=CARTESIAN_POINT ( 'NONE',  ( -108.5228709571501042, -24.66019654487200441, 8.947790411086113949 ) ) ;
#60855=CARTESIAN_POINT ( 'NONE',  ( -100.6305679976983356, -24.40034930558990567, 0.3402023900116026844 ) ) ;
#60856=CARTESIAN_POINT ( 'NONE',  ( -17.86923650574433609, -7.721772263035739492, -1.500000000000002220 ) ) ;
#60858=CARTESIAN_POINT ( 'NONE',  ( -19.99122433398336440, 7.574256484821010105, -1.500000000000002220 ) ) ;
#60860=CARTESIAN_POINT ( 'NONE',  ( -89.80413383862705246, -25.26877915520014639, 5.947789088310639904 ) ) ;
#60862=CARTESIAN_POINT ( 'NONE',  ( -36.62287095715006302, -23.96177878511307568, 10.65340807706330928 ) ) ;
#60863=CARTESIAN_POINT ( 'NONE',  ( -18.74212433040710479, 12.77821124017617649, -1.500000000000002220 ) ) ;
#60865=CARTESIAN_POINT ( 'NONE',  ( -87.52287095715004739, -24.51387760970724727, 9.387446482453409402 ) ) ;
#60866=CARTESIAN_POINT ( 'NONE',  ( -41.22287095715006444, -23.47596703998600631, 11.44779298504227683 ) ) ;
#60867=CARTESIAN_POINT ( 'NONE',  ( -12.28770250403618114, -15.54288071925545722, 11.49999999999999645 ) ) ;
#60869=ORIENTED_EDGE ( 'NONE', *, *, #85319, .T. ) ;
#60870=CARTESIAN_POINT ( 'NONE',  ( -68.58953762381671027, -24.66019654487199375, 8.947790411086124607 ) ) ;
#60872=CARTESIAN_POINT ( 'NONE',  ( -12.93760099376155104, 17.33828479246177423, 11.49999999999998934 ) ) ;
#60873=CARTESIAN_POINT ( 'NONE',  ( -99.62287095715005592, -23.48783264082478794, -1.443836473390061936 ) ) ;
#60874=CARTESIAN_POINT ( 'NONE',  ( -19.30698013599780083, -2.078282243779251637, -1.500000000000002220 ) ) ;
#60875=CARTESIAN_POINT ( 'NONE',  ( -114.5562042904833504, -24.64965694238575011, 8.947790433994187609 ) ) ;
#60876=FACE_OUTER_BOUND ( 'NONE', #79265, .T. ) ;
#60877=CARTESIAN_POINT ( 'NONE',  ( 9.171884637996585710, -17.55225146786146695, -1.500000000000002220 ) ) ;
#60878=ORIENTED_EDGE ( 'NONE', *, *, #27890, .F. ) ;
#60879=CARTESIAN_POINT ( 'NONE',  ( 18.28078834835902455, 8.925752885971231620, 11.49999999999999645 ) ) ;
#60880=CARTESIAN_POINT ( 'NONE',  ( -106.6228709571500559, -29.50250243563736774, 8.947779886222136270 ) ) ;
#60884=VERTEX_POINT ( 'NONE', #37850 ) ;
#60885=CARTESIAN_POINT ( 'NONE',  ( -102.5888613629790882, -24.35071581493543391, 9.817618358456027039 ) ) ;
#60886=CARTESIAN_POINT ( 'NONE',  ( -95.52287095715010423, -24.14406661686761524, 10.28769366194074841 ) ) ;
#60887=CARTESIAN_POINT ( 'NONE',  ( -96.62287095715005592, -23.47596703998600631, 11.44779298504227860 ) ) ;
#60889=CARTESIAN_POINT ( 'NONE',  ( -40.48992741903451531, -24.40133493613049609, 9.663955038902802386 ) ) ;
#60892=CARTESIAN_POINT ( 'NONE',  ( -6.237196068801617699, -19.06703463882530158, -1.500000000000002220 ) ) ;
#60893=B_SPLINE_CURVE_WITH_KNOTS ( 'NONE', 3,
 ( #32325, #94216, #56688, #879 ),
 .UNSPECIFIED., .F., .F.,
 ( 4, 4 ),
 ( 0.000000000000000000, 0.0001000000000000028644 ),
 .UNSPECIFIED. ) ;
#60898=EDGE_CURVE ( 'NONE', #52727, #76836, #12456, .T. ) ;
#60899=EDGE_CURVE ( 'NONE', #63331, #60884, #60819, .T. ) ;
#60900=CARTESIAN_POINT ( 'NONE',  ( 18.88093902437788785, 12.95799798663108682, 11.49999999999999645 ) ) ;
#60901=CARTESIAN_POINT ( 'NONE',  ( -22.72798930328562150, -0.2126449523330483371, 11.49999999999998934 ) ) ;
#60902=CARTESIAN_POINT ( 'NONE',  ( -105.6228709571500559, -23.47593901973091235, -1.443836447538999312 ) ) ;
#60903=CARTESIAN_POINT ( 'NONE',  ( -97.62287095715005592, -23.47593901973091235, -1.443836447539001089 ) ) ;
#60904=CARTESIAN_POINT ( 'NONE',  ( -35.52287095715006870, -29.50248528299804818, 1.056150453629031594 ) ) ;
#60905=ADVANCED_FACE ( 'NONE', ( #68305 ), #98745, .T. ) ;
#60907=CARTESIAN_POINT ( 'NONE',  ( -31.62287095715005236, -23.47593901973091235, -1.443836447539013301 ) ) ;
#60910=CARTESIAN_POINT ( 'NONE',  ( -20.29798418530817017, 1.744846428065259136, 11.49999999999998934 ) ) ;
#60913=CARTESIAN_POINT ( 'NONE',  ( 13.56796309060646166, -18.52494293750034871, 11.49999999999998934 ) ) ;
#60915=ORIENTED_EDGE ( 'NONE', *, *, #82881, .T. ) ;
#60916=CARTESIAN_POINT ( 'NONE',  ( -108.5864047394081950, -24.66019654487200441, 8.947790411086108620 ) ) ;
#60917=CARTESIAN_POINT ( 'NONE',  ( -77.50092983151746751, -24.51419770103158768, 9.386484678747166299 ) ) ;
#60920=CARTESIAN_POINT ( 'NONE',  ( -3.120219904758775975, 21.05623772282662998, 11.49999999999999645 ) ) ;
#60921=EDGE_LOOP ( 'NONE', ( #96639, #22595, #66122, #28261 ) ) ;
#60922=VERTEX_POINT ( 'NONE', #91626 ) ;
#60923=CARTESIAN_POINT ( 'NONE',  ( 5.796264663052079769, -21.44337444023769379, -1.500000000000002220 ) ) ;
#60924=CARTESIAN_POINT ( 'NONE',  ( -0.003042231299257275486, -20.61035990087709635, 11.49999999999998934 ) ) ;
#60925=EDGE_CURVE ( 'NONE', #100062, #1418, #88670, .T. ) ;
#60926=B_SPLINE_CURVE_WITH_KNOTS ( 'NONE', 3,
 ( #95368, #39581, #55825, #86257 ),
 .UNSPECIFIED., .F., .F.,
 ( 4, 4 ),
 ( 0.8103645859926805750, 0.8193710172647959977 ),
 .UNSPECIFIED. ) ;
#60932=ORIENTED_EDGE ( 'NONE', *, *, #22244, .F. ) ;
#60933=CARTESIAN_POINT ( 'NONE',  ( -124.7735416517568723, -25.27125674707836822, 4.078964885054434220 ) ) ;
#60934=DIRECTION ( 'NONE',  ( 0.000000000000000000, 2.173523156925980399E-06, -0.9999999999976378895 ) ) ;
#60935=CARTESIAN_POINT ( 'NONE',  ( 20.25184064777635484, 4.944226511633750043, -1.500000000000002220 ) ) ;
#60936=CARTESIAN_POINT ( 'NONE',  ( -11.04117723084791614, -18.81814233335528286, 11.49999999999999645 ) ) ;
#60938=CARTESIAN_POINT ( 'NONE',  ( -78.62655469335055614, -24.51419770103157347, 9.386484678747175181 ) ) ;
#60939=CARTESIAN_POINT ( 'NONE',  ( 19.77452139984142221, -10.64395493966388706, 11.49999999999998934 ) ) ;
#60949=DIRECTION ( 'NONE',  ( 1.000000000000000000, 3.773278334444166432E-23, 8.201307841325785021E-29 ) ) ;
#60951=VECTOR ( 'NONE', #80992, 1000.000000000000227 ) ;
#60952=CARTESIAN_POINT ( 'NONE',  ( 5.124585555570928541, 20.71496159572455653, -1.500000000000002220 ) ) ;
#60954=AXIS2_PLACEMENT_3D ( 'NONE', #78128, #46711, #61439 ) ;
#60955=CARTESIAN_POINT ( 'NONE',  ( -9.798014431990228701, 18.61115389415964572, -1.500000000000002220 ) ) ;
#60956=FACE_OUTER_BOUND ( 'NONE', #81127, .T. ) ;
#60957=CARTESIAN_POINT ( 'NONE',  ( -111.1735661057252145, -25.24499744434313442, 3.690036886848450770 ) ) ;
#60958=AXIS2_PLACEMENT_3D ( 'NONE', #33035, #7809, #49777 ) ;
#60960=CARTESIAN_POINT ( 'NONE',  ( -3.625624329714521643, -21.66436044012089468, -1.500000000000002220 ) ) ;
#60961=CARTESIAN_POINT ( 'NONE',  ( -87.55456245514183422, -23.96119346886881729, -0.6495511937831870419 ) ) ;
#60962=ORIENTED_EDGE ( 'NONE', *, *, #49163, .F. ) ;
#60964=B_SPLINE_CURVE_WITH_KNOTS ( 'NONE', 3,
 ( #25820, #26322, #11092, #56292 ),
 .UNSPECIFIED., .F., .F.,
 ( 4, 4 ),
 ( 0.000000000000000000, 9.999999999998897304E-05 ),
 .UNSPECIFIED. ) ;
#60967=CARTESIAN_POINT ( 'NONE',  ( -84.50374581864701895, -24.51419770103157347, 9.386484678747175181 ) ) ;
#60968=DIRECTION ( 'NONE',  ( -3.773278334453079618E-23, 0.9999999999976377785, 2.173523156925979975E-06 ) ) ;
#60969=CARTESIAN_POINT ( 'NONE',  ( -20.42746634971195974, -23.78597006378213408, 9.174899246800713115 ) ) ;
#60970=CARTESIAN_POINT ( 'NONE',  ( 7.794017451908327843, -19.83292067980804774, -1.500000000000002220 ) ) ;
#60971=CARTESIAN_POINT ( 'NONE',  ( -98.51384325196762859, -24.15620529776628445, 10.23563542870660292 ) ) ;
#60973=PLANE ( 'NONE',  #56826 ) ;
#60974=CARTESIAN_POINT ( 'NONE',  ( -33.52200586597940912, -23.48783264082477729, -1.443836473390078146 ) ) ;
#60975=CARTESIAN_POINT ( 'NONE',  ( -22.07377061809603092, 4.253497373390751513, -1.500000000000002220 ) ) ;
#60976=CARTESIAN_POINT ( 'NONE',  ( -108.8772486938376289, -25.21970293610405633, 6.713732480141158199 ) ) ;
#60977=VERTEX_POINT ( 'NONE', #30735 ) ;
#60979=CARTESIAN_POINT ( 'NONE',  ( -19.37001648656083574, -3.113731218521536004, 11.49999999999999645 ) ) ;
#60980=CARTESIAN_POINT ( 'NONE',  ( -68.62287095715001328, -24.33832256526968862, 0.1851278514119885088 ) ) ;
#60981=FACE_OUTER_BOUND ( 'NONE', #82120, .T. ) ;
#60982=EDGE_LOOP ( 'NONE', ( #17593, #71541, #35254, #93644 ) ) ;
#60983=DIRECTION ( 'NONE',  ( -3.773278334453079618E-23, 0.9999999999976377785, 2.173523156925979975E-06 ) ) ;
#60984=CARTESIAN_POINT ( 'NONE',  ( -84.52287095715006160, -23.47593901973090524, -1.443836447538996648 ) ) ;
#60985=CARTESIAN_POINT ( 'NONE',  ( -124.5194944430484014, -24.66019654487200441, 8.947790411086108620 ) ) ;
#60988=CARTESIAN_POINT ( 'NONE',  ( -19.65353550717971487, 1.628721094194526486, 11.49999999999998934 ) ) ;
#60994=CARTESIAN_POINT ( 'NONE',  ( -47.62287095715004170, -24.65952944569304250, 1.056160979905693686 ) ) ;
#60995=CARTESIAN_POINT ( 'NONE',  ( -69.62287095715005592, -24.66019654487199020, 8.947790411086131712 ) ) ;
#60997=CARTESIAN_POINT ( 'NONE',  ( -66.52287095715007581, -23.47593901973090524, -1.443836447538997092 ) ) ;
#61000=B_SPLINE_CURVE_WITH_KNOTS ( 'NONE', 3,
 ( #18550, #40891, #49522, #80454 ),
 .UNSPECIFIED., .F., .F.,
 ( 4, 4 ),
 ( 0.000000000000000000, 9.999999999998897304E-05 ),
 .UNSPECIFIED. ) ;
#61001=CARTESIAN_POINT ( 'NONE',  ( -95.52287095715006160, -23.47596703998600631, 11.44779298504228215 ) ) ;
#61003=CARTESIAN_POINT ( 'NONE',  ( -107.5594696158587595, -23.48783264082479505, -1.443836473390060826 ) ) ;
#61004=CARTESIAN_POINT ( 'NONE',  ( -17.55682386033230102, 9.526633247210019917, -1.500000000000002220 ) ) ;
#61006=CARTESIAN_POINT ( 'NONE',  ( -125.6228709571500843, -25.00182538069146432, 7.747789668545100206 ) ) ;
#61007=CARTESIAN_POINT ( 'NONE',  ( -45.49983799985675148, -24.15602025860896163, 10.28564288303535434 ) ) ;
#61014=CARTESIAN_POINT ( 'NONE',  ( -39.49146858854847864, -24.34968618360933235, 0.1864209137778788106 ) ) ;
#61016=CARTESIAN_POINT ( 'NONE',  ( -51.09576285965076181, -25.31574456684156615, 4.912418940310026017 ) ) ;
#61017=CARTESIAN_POINT ( 'NONE',  ( -64.62287095715002749, -23.73907113216990084, -1.053371485793233475 ) ) ;
#61019=DIRECTION ( 'NONE',  ( -3.773278334453079618E-23, 0.9999999999976377785, 2.173523156925979975E-06 ) ) ;
#61021=ORIENTED_EDGE ( 'NONE', *, *, #39827, .T. ) ;
#61023=CARTESIAN_POINT ( 'NONE',  ( -12.21837793623082113, -16.16665877782589433, 11.49999999999998934 ) ) ;
#61024=CARTESIAN_POINT ( 'NONE',  ( -122.6234929783657890, -24.65952944569305316, 1.056160979905708786 ) ) ;
#61027=CARTESIAN_POINT ( 'NONE',  ( -90.52287095715009002, -24.62226745350443480, 0.9660975649729555137 ) ) ;
#61028=ORIENTED_EDGE ( 'NONE', *, *, #69043, .T. ) ;
#61029=DIRECTION ( 'NONE',  ( -3.773278334444167608E-23, 1.000000000000000000, 0.000000000000000000 ) ) ;
#61031=CARTESIAN_POINT ( 'NONE',  ( 18.22116949570664701, -8.484823103377051368, -1.500000000000002220 ) ) ;
#61032=CARTESIAN_POINT ( 'NONE',  ( -13.06023916655064276, -16.53025015627232719, 11.49999999999999645 ) ) ;
#61033=B_SPLINE_CURVE_WITH_KNOTS ( 'NONE', 3,
 ( #80005, #80507, #18112, #85742, #79506, #9994 ),
 .UNSPECIFIED., .F., .F.,
 ( 4, 2, 4 ),
 ( 1.570755371633954459E-05, 0.001396183895866086669, 0.002776660238015833844 ),
 .UNSPECIFIED. ) ;
#61034=CARTESIAN_POINT ( 'NONE',  ( -99.58953762381672448, -24.64965694238407323, 8.947790433994651238 ) ) ;
#61035=CARTESIAN_POINT ( 'NONE',  ( -2.366842300981895519, -21.98859952056468714, 11.49999999999998934 ) ) ;
#61036=CARTESIAN_POINT ( 'NONE',  ( 16.23509277041898358, 12.58620111108425377, 11.49999999999998934 ) ) ;
#61038=VERTEX_POINT ( 'NONE', #17002 ) ;
#61041=CARTESIAN_POINT ( 'NONE',  ( -82.92287095715005307, -23.47596703998600631, 11.44779298504227860 ) ) ;
#61042=B_SPLINE_CURVE_WITH_KNOTS ( 'NONE', 3,
 ( #76038, #6039, #91764, #45119, #82663, #83156, #36991, #45612 ),
 .UNSPECIFIED., .F., .F.,
 ( 4, 2, 2, 4 ),
 ( 6.384118678612463891E-06, 0.002007151183507257554, 0.003007534715921580341, 0.004007918248335903127 ),
 .UNSPECIFIED. ) ;
#61043=FACE_OUTER_BOUND ( 'NONE', #24710, .T. ) ;
#61045=ORIENTED_EDGE ( 'NONE', *, *, #6760, .T. ) ;
#61047=PLANE ( 'NONE',  #38888 ) ;
#61048=CARTESIAN_POINT ( 'NONE',  ( -71.62287095715005592, -23.47596703998600631, 11.44779298504227683 ) ) ;
#61049=CARTESIAN_POINT ( 'NONE',  ( -28.52287095715005805, -29.50250786944459946, 11.44777958301664356 ) ) ;
#61050=CARTESIAN_POINT ( 'NONE',  ( -20.60669311552257810, 0.8253496925510150906, -1.500000000000002220 ) ) ;
#61051=CARTESIAN_POINT ( 'NONE',  ( 15.46703529437019853, -15.08741104398349187, 11.49999999999999645 ) ) ;
#61052=VERTEX_POINT ( 'NONE', #1791 ) ;
#61053=CARTESIAN_POINT ( 'NONE',  ( -46.52287095715006160, -24.64965694238406613, 8.947790433994203596 ) ) ;
#61054=EDGE_CURVE ( 'NONE', #58570, #72031, #78937, .T. ) ;
#61055=VECTOR ( 'NONE', #36715, 1000.000000000000114 ) ;
#61057=CARTESIAN_POINT ( 'NONE',  ( -22.26391555059773353, 2.265117081278330780, -1.500000000000002220 ) ) ;
#61058=CARTESIAN_POINT ( 'NONE',  ( -34.52287095715006160, -24.35013146730202749, 9.818937971375103047 ) ) ;
#61059=CARTESIAN_POINT ( 'NONE',  ( -84.52214531569265432, -23.48783264082476308, -1.443836473390094799 ) ) ;
#61061=B_SPLINE_CURVE_WITH_KNOTS ( 'NONE', 3,
 ( #90276, #29870, #67951, #12645 ),
 .UNSPECIFIED., .F., .F.,
 ( 4, 4 ),
 ( 4.163336342344337027E-17, 9.999999999997512235E-05 ),
 .UNSPECIFIED. ) ;
#61062=CARTESIAN_POINT ( 'NONE',  ( -100.0601433209239133, -25.31017654890569801, 4.635600862196024963 ) ) ;
#61063=CARTESIAN_POINT ( 'NONE',  ( -35.62380681592568266, -25.00182538069146787, 7.747789668545037145 ) ) ;
#61065=CARTESIAN_POINT ( 'NONE',  ( -3.950822543831816080, -20.53616823614468956, 11.49999999999998934 ) ) ;
#61066=ORIENTED_EDGE ( 'NONE', *, *, #32875, .F. ) ;
#61067=ADVANCED_FACE ( 'NONE', ( #9892 ), #87529, .F. ) ;
#61068=CARTESIAN_POINT ( 'NONE',  ( -67.64622146058944452, -23.73791477778911840, 11.05961554403170766 ) ) ;
#61071=CARTESIAN_POINT ( 'NONE',  ( -50.62287095715007723, -24.91570333823099759, 8.075032458375556388 ) ) ;
#61072=CARTESIAN_POINT ( 'NONE',  ( 19.29917393477590437, 8.764703196630867055, -1.500000000000002220 ) ) ;
#61073=ORIENTED_EDGE ( 'NONE', *, *, #51492, .F. ) ;
#61076=CARTESIAN_POINT ( 'NONE',  ( 21.67628855941699939, -2.339797445609365756, 11.49999999999998934 ) ) ;
#61077=DIRECTION ( 'NONE',  ( 0.000000000000000000, -2.173523156925980399E-06, 0.9999999999976378895 ) ) ;
#61078=CARTESIAN_POINT ( 'NONE',  ( -36.62287095715004881, -24.33832256527048088, 0.1851278514138546272 ) ) ;
#61080=CARTESIAN_POINT ( 'NONE',  ( 19.96715809174937561, -8.635335823514383335, -1.500000000000002220 ) ) ;
#61082=CARTESIAN_POINT ( 'NONE',  ( 8.793911523065595759, -20.50603677605392150, 11.49999999999999645 ) ) ;
#61084=CARTESIAN_POINT ( 'NONE',  ( -33.52287095715004739, -24.34917612407030063, 0.1852690917476907950 ) ) ;
#61086=CARTESIAN_POINT ( 'NONE',  ( -56.62287095715005592, -29.50250243563736774, 8.947779886222145151 ) ) ;
#61088=AXIS2_PLACEMENT_3D ( 'NONE', #56865, #18769, #49751 ) ;
#61090=ORIENTED_EDGE ( 'NONE', *, *, #41062, .F. ) ;
#61092=CARTESIAN_POINT ( 'NONE',  ( 15.88363568188429653, -14.04911357082368006, -1.500000000000002220 ) ) ;
#61094=CARTESIAN_POINT ( 'NONE',  ( -80.47485683444980964, -25.27791972877900406, 7.562833136764695929 ) ) ;
#61097=DIRECTION ( 'NONE',  ( -3.773278334453080206E-23, 0.9999999999976377785, 2.173523156925979975E-06 ) ) ;
#61098=B_SPLINE_CURVE_WITH_KNOTS ( 'NONE', 3,
 ( #36210, #21952, #43331, #4761, #52937, #67174 ),
 .UNSPECIFIED., .F., .F.,
 ( 4, 2, 4 ),
 ( 1.570755371633797249E-05, 0.001396183895866087536, 0.002776660238015836880 ),
 .UNSPECIFIED. ) ;
#61099=CARTESIAN_POINT ( 'NONE',  ( -5.798782886354239885, 18.49141925852020663, 11.49999999999998934 ) ) ;
#61100=CARTESIAN_POINT ( 'NONE',  ( -45.61118087450132919, -23.85016227208580375, -0.8807180028928391913 ) ) ;
#61101=VERTEX_POINT ( 'NONE', #40843 ) ;
#61103=CARTESIAN_POINT ( 'NONE',  ( -5.694372300836820777, 18.57635362771370424, 11.49999999999999645 ) ) ;
#61106=ORIENTED_EDGE ( 'NONE', *, *, #29511, .T. ) ;
#61107=CARTESIAN_POINT ( 'NONE',  ( -78.55620429048340725, -23.47596703998600276, 11.44779298504227683 ) ) ;
#61109=CARTESIAN_POINT ( 'NONE',  ( -121.5228709571500616, -23.47596703998600631, 11.44779298504227860 ) ) ;
#61110=EDGE_CURVE ( 'NONE', #58493, #72155, #80027, .T. ) ;
#61111=CARTESIAN_POINT ( 'NONE',  ( -19.61951575358169819, -0.1233725505697131491, -1.500000000000002220 ) ) ;
#61112=FACE_OUTER_BOUND ( 'NONE', #95477, .T. ) ;
#61113=ORIENTED_EDGE ( 'NONE', *, *, #29999, .F. ) ;
#61114=CARTESIAN_POINT ( 'NONE',  ( 21.48638754631891246, 1.654510534108022179, 11.49999999999998934 ) ) ;
#61115=CARTESIAN_POINT ( 'NONE',  ( -33.54540960989195497, -24.15620529776627379, 10.23563542870661536 ) ) ;
#61118=CARTESIAN_POINT ( 'NONE',  ( 11.92049557817732364, -19.74369927386287671, -1.500000000000002220 ) ) ;
#61119=B_SPLINE_CURVE_WITH_KNOTS ( 'NONE', 3,
 ( #64353, #73443, #79543, #10033, #18144, #3937 ),
 .UNSPECIFIED., .F., .F.,
 ( 4, 2, 4 ),
 ( 6.391158118967745954E-06, 0.001387004593080787230, 0.002767618028042606766 ),
 .UNSPECIFIED. ) ;
#61120=B_SPLINE_CURVE_WITH_KNOTS ( 'NONE', 3,
 ( #60805, #15604, #52182, #75998, #46568, #91232 ),
 .UNSPECIFIED., .F., .F.,
 ( 4, 2, 4 ),
 ( 0.000000000000000000, 0.001380901958385391580, 0.002761803916770783161 ),
 .UNSPECIFIED. ) ;
#61123=CARTESIAN_POINT ( 'NONE',  ( -50.70339841325804997, -25.29249258120279009, 4.255736650380444352 ) ) ;
#61124=CARTESIAN_POINT ( 'NONE',  ( 14.71488472389458124, -13.84269218943631508, 11.49999999999999645 ) ) ;
#61125=CARTESIAN_POINT ( 'NONE',  ( -121.6245712669088732, -24.35071581493543391, 9.817618358456025263 ) ) ;
#61126=CARTESIAN_POINT ( 'NONE',  ( -91.52287095715006160, -24.51283580621365488, 0.6167428607019749265 ) ) ;
#61127=EDGE_CURVE ( 'NONE', #18110, #85110, #57590, .T. ) ;
#61128=CARTESIAN_POINT ( 'NONE',  ( -111.7788625685672486, -25.10921688335350055, 4.278827964032922537 ) ) ;
#61131=CARTESIAN_POINT ( 'NONE',  ( -110.9011049686103263, -25.29779188398908829, 3.445933212628501163 ) ) ;
#61132=CARTESIAN_POINT ( 'NONE',  ( 17.57725459251073019, -9.329341740261039462, 11.49999999999998934 ) ) ;
#61134=CARTESIAN_POINT ( 'NONE',  ( -79.11611000704998276, -25.16711686381824720, 3.101159594853582835 ) ) ;
#61135=CARTESIAN_POINT ( 'NONE',  ( 0.5484783294719396407, -19.75002165935583776, -1.500000000000002220 ) ) ;
#61137=CARTESIAN_POINT ( 'NONE',  ( -56.65737350661340344, -23.48783264082477018, -1.443836473390095909 ) ) ;
#61138=ADVANCED_FACE ( 'NONE', ( #33739 ), #56594, .T. ) ;
#61139=ADVANCED_FACE ( 'NONE', ( #17509 ), #63713, .F. ) ;
#61140=PLANE ( 'NONE',  #64652 ) ;
#61141=LINE ( 'NONE', #59644, #88063 ) ;
#61142=CARTESIAN_POINT ( 'NONE',  ( 17.27521350410721368, -11.31798593588896829, 11.49999999999999645 ) ) ;
#61143=VECTOR ( 'NONE', #71837, 1000.000000000000114 ) ;
#61144=LINE ( 'NONE', #38278, #95358 ) ;
#61145=ADVANCED_FACE ( 'NONE', ( #88527 ), #42565, .T. ) ;
#61146=B_SPLINE_CURVE_WITH_KNOTS ( 'NONE', 3,
 ( #25184, #40424, #59518, #63785, #79976, #71381 ),
 .UNSPECIFIED., .F., .F.,
 ( 4, 2, 4 ),
 ( 0.000000000000000000, 0.001380901958385385509, 0.002761803916770771018 ),
 .UNSPECIFIED. ) ;
#61147=CARTESIAN_POINT ( 'NONE',  ( -119.6228709571500559, -29.50250243563736774, 8.947779886222134493 ) ) ;
#61148=CARTESIAN_POINT ( 'NONE',  ( 9.008567143757492346, 20.83016157428379955, 11.49999999999999645 ) ) ;
#61150=B_SPLINE_SURFACE_WITH_KNOTS ( 'NONE', 3, 1, ( 
 ( #84927, #93530 ),
 ( #70213, #84429 ),
 ( #93032, #62609 ),
 ( #24026, #76798 ),
 ( #30645, #45882 ),
 ( #68718, #23510 ),
 ( #78308, #99634 ),
 ( #54995, #92536 ),
 ( #85935, #30138 ),
 ( #39750, #53506 ),
 ( #70710, #7298 ),
 ( #38250, #23009 ),
 ( #28469, #36092 ),
 ( #69035, #43708 ),
 ( #37588, #5635 ),
 ( #75145, #91368 ),
 ( #36581, #21843 ),
 ( #68539, #51320 ),
 ( #59434, #14233 ) ),
 .UNSPECIFIED., .F., .F., .F.,
 ( 4, 1, 1, 1, 1, 1, 1, 1, 1, 1, 1, 1, 1, 1, 1, 1, 4 ),
 ( 2, 2 ),
 ( 0.000000000000000000, 0.05953958549708775888, 0.1174229600021179099, 0.1744404410469199418, 0.2317338905564219620, 0.2897219772859587206, 0.3492003964486030121, 0.4105155317344490462, 0.4750802789743625576, 0.5400944754761672906, 0.6044440959297832094, 0.6686966743402348312, 0.7321102011010777177, 0.7967393467417489550, 0.8629057297096498491, 0.9304616390764175460, 0.9999999999999998890 ),
 ( 0.000000000000000000, 1.000000000000000000 ),
 .UNSPECIFIED. ) ;
#61151=DIRECTION ( 'NONE',  ( 3.773278334444167608E-23, -1.000000000000000000, 0.000000000000000000 ) ) ;
#61152=CARTESIAN_POINT ( 'NONE',  ( -33.62287095715005592, -24.66019654487199020, 8.947790411086138818 ) ) ;
#61153=CARTESIAN_POINT ( 'NONE',  ( 8.007726535620864894, 18.53121347637897287, -1.500000000000002220 ) ) ;
#61155=CARTESIAN_POINT ( 'NONE',  ( -111.7814946224345789, -25.29712067403330877, 4.332404411321261861 ) ) ;
#61156=B_SPLINE_CURVE_WITH_KNOTS ( 'NONE', 3,
 ( #53928, #23956, #7737, #54923, #84859, #38683 ),
 .UNSPECIFIED., .F., .F.,
 ( 4, 2, 4 ),
 ( 0.000000000000000000, 0.001380764517854763014, 0.002761529035709526028 ),
 .UNSPECIFIED. ) ;
#61158=ORIENTED_EDGE ( 'NONE', *, *, #54752, .T. ) ;
#61160=B_SPLINE_CURVE_WITH_KNOTS ( 'NONE', 3,
 ( #95657, #73326, #80930, #81926, #72325, #57608 ),
 .UNSPECIFIED., .F., .F.,
 ( 4, 2, 4 ),
 ( 1.570755371634150632E-05, 0.001396183895866087319, 0.002776660238015833410 ),
 .UNSPECIFIED. ) ;
#61163=CARTESIAN_POINT ( 'NONE',  ( 21.13568926591755925, -8.834425160694816981, 11.49999999999998934 ) ) ;
#61165=CARTESIAN_POINT ( 'NONE',  ( 19.51036611237648088, 9.378288983258578071, -1.500000000000002220 ) ) ;
#61166=DIRECTION ( 'NONE',  ( -3.773278334444167608E-23, 1.000000000000000000, 0.000000000000000000 ) ) ;
#61167=DIRECTION ( 'NONE',  ( 0.000000000000000000, -2.173523156925980399E-06, 0.9999999999976378895 ) ) ;
#61168=CARTESIAN_POINT ( 'NONE',  ( -16.13976855045889636, 13.32451261336467496, 11.49999999999999645 ) ) ;
#61169=ORIENTED_EDGE ( 'NONE', *, *, #42014, .T. ) ;
#61170=CARTESIAN_POINT ( 'NONE',  ( -124.5904483378009218, -23.96119346886880308, -0.6495511937832024740 ) ) ;
#61171=CARTESIAN_POINT ( 'NONE',  ( -15.57331531552114612, -15.56871402003811333, 11.49999999999998934 ) ) ;
#61173=CARTESIAN_POINT ( 'NONE',  ( -105.5884166583201988, -24.63419186844610920, 9.035850630976920428 ) ) ;
#61174=CARTESIAN_POINT ( 'NONE',  ( -28.66268959117890347, -25.21724901141872976, 7.176256802127888967 ) ) ;
#61175=ORIENTED_EDGE ( 'NONE', *, *, #26536, .T. ) ;
#61176=PLANE ( 'NONE',  #28010 ) ;
#61177=CARTESIAN_POINT ( 'NONE',  ( -90.60546021415382256, -23.48786465467241058, 11.44779295918254824 ) ) ;
#61179=CARTESIAN_POINT ( 'NONE',  ( -72.51646068626162389, -23.73791477778911840, 11.05961554403170943 ) ) ;
#61180=ORIENTED_EDGE ( 'NONE', *, *, #79430, .F. ) ;
#61182=VERTEX_POINT ( 'NONE', #20003 ) ;
#61183=CARTESIAN_POINT ( 'NONE',  ( -102.6228709571500559, -29.50247984919015209, -1.443849546365050029 ) ) ;
#61184=CARTESIAN_POINT ( 'NONE',  ( -117.5228709571500758, -24.64965694238408034, 8.947790433994191162 ) ) ;
#61185=CARTESIAN_POINT ( 'NONE',  ( -100.5228709571500616, -24.82576562948881005, 8.398263436605667209 ) ) ;
#61186=CARTESIAN_POINT ( 'NONE',  ( 20.39306652673287701, -2.074774109220689500, -1.500000000000002220 ) ) ;
#61188=VERTEX_POINT ( 'NONE', #13377 ) ;
#61190=CARTESIAN_POINT ( 'NONE',  ( -30.61048516611183956, -24.43626637953623160, 0.1835287498755953095 ) ) ;
#61192=CARTESIAN_POINT ( 'NONE',  ( 22.20168578472828358, 1.497490109320031682, 11.49999999999998934 ) ) ;
#61193=EDGE_CURVE ( 'NONE', #81664, #55675, #5278, .T. ) ;
#61194=CARTESIAN_POINT ( 'NONE',  ( -98.52287095715006160, -24.65952944569304606, 1.056160979905702346 ) ) ;
#61196=ORIENTED_EDGE ( 'NONE', *, *, #77187, .F. ) ;
#61198=CARTESIAN_POINT ( 'NONE',  ( -28.41099462919338237, -24.63646035822953451, 8.118938870972160160 ) ) ;
#61199=CARTESIAN_POINT ( 'NONE',  ( 9.628234360240019996, 18.42577530400075858, 11.49999999999998934 ) ) ;
#61200=EDGE_LOOP ( 'NONE', ( #73171, #72377, #65413, #55487 ) ) ;
#61202=ORIENTED_EDGE ( 'NONE', *, *, #81532, .T. ) ;
#61203=CARTESIAN_POINT ( 'NONE',  ( -31.55620429048339304, -24.65952944569304606, 1.056160979905691688 ) ) ;
#61204=EDGE_CURVE ( 'NONE', #56477, #44828, #18382, .T. ) ;
#61205=ORIENTED_EDGE ( 'NONE', *, *, #44755, .T. ) ;
#61206=ORIENTED_EDGE ( 'NONE', *, *, #91533, .T. ) ;
#61209=CARTESIAN_POINT ( 'NONE',  ( -116.5120815788254021, -25.30053193007086065, 4.607778174927533499 ) ) ;
#61210=CARTESIAN_POINT ( 'NONE',  ( -40.62287095715006302, -24.15516710230294350, 10.28746687063726029 ) ) ;
#61211=CARTESIAN_POINT ( 'NONE',  ( -109.4104630438534542, -25.17367207030539689, 3.148482298596714024 ) ) ;
#61212=LINE ( 'NONE', #92132, #27052 ) ;
#61213=CARTESIAN_POINT ( 'NONE',  ( 1.014068502963303864, -22.09113584270698993, 11.49999999999999645 ) ) ;
#61214=EDGE_LOOP ( 'NONE', ( #88792, #97439, #63681, #61695 ) ) ;
#61215=EDGE_CURVE ( 'NONE', #41031, #58438, #7402, .T. ) ;
#61217=CARTESIAN_POINT ( 'NONE',  ( -15.40814491850785650, 16.58152744545821022, 11.49999999999998934 ) ) ;
#61219=CARTESIAN_POINT ( 'NONE',  ( -29.16552315785632743, -25.14802933280332198, 6.095404567958068398 ) ) ;
#61221=ORIENTED_EDGE ( 'NONE', *, *, #28732, .F. ) ;
#61224=CARTESIAN_POINT ( 'NONE',  ( -2.706554608146168217, 19.95013100808389339, 11.49999999999998934 ) ) ;
#61226=VERTEX_POINT ( 'NONE', #21482 ) ;
#61228=CARTESIAN_POINT ( 'NONE',  ( 16.41691039316204481, 15.16158741987741365, -1.500000000000002220 ) ) ;
#61229=ORIENTED_EDGE ( 'NONE', *, *, #27996, .F. ) ;
#61230=ORIENTED_EDGE ( 'NONE', *, *, #41936, .T. ) ;
#61231=CARTESIAN_POINT ( 'NONE',  ( -34.92287095715007439, -23.47593901973090524, -1.443836447538998646 ) ) ;
#61232=DIRECTION ( 'NONE',  ( -3.773278334444166432E-23, 1.000000000000000000, 0.000000000000000000 ) ) ;
#61237=CARTESIAN_POINT ( 'NONE',  ( 18.00893756148942870, 7.586210683597776949, -1.500000000000002220 ) ) ;
#61238=CARTESIAN_POINT ( 'NONE',  ( -102.5228709571501042, -23.48783264083375144, -1.443836473376139740 ) ) ;
#61239=CARTESIAN_POINT ( 'NONE',  ( 1.049947104896167049, -21.43676768134831434, -1.500000000000002220 ) ) ;
#61243=CARTESIAN_POINT ( 'NONE',  ( -17.51315278866654879, 14.73147661606379621, -1.500000000000002220 ) ) ;
#61244=AXIS2_PLACEMENT_3D ( 'NONE', #31585, #85879, #23967 ) ;
#61246=FACE_OUTER_BOUND ( 'NONE', #48312, .T. ) ;
#61248=CARTESIAN_POINT ( 'NONE',  ( 19.98059151383774434, -0.7942727526097331792, 11.49999999999999645 ) ) ;
#61249=CARTESIAN_POINT ( 'NONE',  ( -31.62287095715005236, -23.48783264082477729, -1.443836473390074149 ) ) ;
#61253=ADVANCED_FACE ( 'NONE', ( #20493 ), #66713, .F. ) ;
#61254=ORIENTED_EDGE ( 'NONE', *, *, #77490, .F. ) ;
#61256=CARTESIAN_POINT ( 'NONE',  ( -70.52287095715007581, -23.48786465467241769, 11.44779295918254647 ) ) ;
#61257=CARTESIAN_POINT ( 'NONE',  ( -20.56741719582323213, 7.008553436993695485, 11.49999999999998934 ) ) ;
#61258=CARTESIAN_POINT ( 'NONE',  ( -117.5228709571500758, -23.48783264082477729, -1.443836473390083697 ) ) ;
#61259=CARTESIAN_POINT ( 'NONE',  ( -2.459534284235005863, 19.42625828800391119, -1.500000000000002220 ) ) ;
#61260=DIRECTION ( 'NONE',  ( -3.773278334453079618E-23, 0.9999999999976377785, 2.173523156925979975E-06 ) ) ;
#61261=CARTESIAN_POINT ( 'NONE',  ( -109.6940667814372006, -25.31698119913111000, 5.011372319774925366 ) ) ;
#61263=EDGE_CURVE ( 'NONE', #39813, #24849, #2577, .T. ) ;
#61266=CARTESIAN_POINT ( 'NONE',  ( -15.16157141410761966, -13.82251119679066953, 11.49999999999999645 ) ) ;
#61267=CARTESIAN_POINT ( 'NONE',  ( -34.62287095715005592, -29.50247984919015209, -1.443849546365062242 ) ) ;
#61268=EDGE_CURVE ( 'NONE', #54721, #99816, #76410, .T. ) ;
#61270=ORIENTED_EDGE ( 'NONE', *, *, #3964, .T. ) ;
#61272=DIRECTION ( 'NONE',  ( -3.773278334453079030E-23, 0.9999999999976377785, 2.173523156925979128E-06 ) ) ;
#61274=CARTESIAN_POINT ( 'NONE',  ( -125.6264018559343754, -23.48786465467241413, 11.44779295918253581 ) ) ;
#61275=CARTESIAN_POINT ( 'NONE',  ( -85.62287095715001328, -23.85196035786900737, -0.8779234886474913679 ) ) ;
#61276=EDGE_CURVE ( 'NONE', #56269, #31248, #83894, .T. ) ;
#61277=CARTESIAN_POINT ( 'NONE',  ( -85.52287095715004739, -24.63287334234178161, 0.9662140553045371894 ) ) ;
#61279=CARTESIAN_POINT ( 'NONE',  ( -23.05830607064937965, -0.9945063503333604338, 11.49999999999999645 ) ) ;
#61280=CARTESIAN_POINT ( 'NONE',  ( -0.9063223138645676302, -22.79912562917415997, 11.49999999999998934 ) ) ;
#61281=CARTESIAN_POINT ( 'NONE',  ( -74.56445243665983469, -23.48783264082477018, -1.443836473390096353 ) ) ;
#61282=B_SPLINE_SURFACE_WITH_KNOTS ( 'NONE', 3, 3, ( 
 ( #9931, #71845, #94666, #31264 ),
 ( #15533, #318, #40885, #46498 ),
 ( #85549, #32767, #77424, #25148 ),
 ( #70840, #55626, #2335, #56128 ),
 ( #62234, #86556, #16032, #46998 ),
 ( #8432, #11433, #95674, #18046 ),
 ( #87559, #42412, #34778, #10938 ) ),
 .UNSPECIFIED., .F., .F., .F.,
 ( 4, 3, 4 ),
 ( 4, 4 ),
 ( 0.0004766839783849497066, 0.1029713700210913990, 0.2054660560637978362 ),
 ( 0.01949895744967442002, 0.02052067878884997545 ),
 .UNSPECIFIED. ) ;
#61283=CARTESIAN_POINT ( 'NONE',  ( -75.52287095715013265, -24.51254535375842636, 9.355368624242251130 ) ) ;
#61285=CARTESIAN_POINT ( 'NONE',  ( -21.98280116189361877, -4.439423430357301470, 11.49999999999999645 ) ) ;
#61286=CARTESIAN_POINT ( 'NONE',  ( -115.5228709571499905, -24.15431212366390312, -0.2830839119429361395 ) ) ;
#61287=CARTESIAN_POINT ( 'NONE',  ( -110.5109861788922103, -24.92564183028978775, 1.928384488918252204 ) ) ;
#61288=CARTESIAN_POINT ( 'NONE',  ( -19.93956527825925917, 9.129326121205059152, 11.49999999999998934 ) ) ;
#61291=CARTESIAN_POINT ( 'NONE',  ( -40.41683116089613748, -25.31532428806244539, 5.082404371757057504 ) ) ;
#61292=CARTESIAN_POINT ( 'NONE',  ( -49.11047489538273680, -25.15112582127123275, 6.935676789746522353 ) ) ;
#61294=ORIENTED_EDGE ( 'NONE', *, *, #83892, .T. ) ;
#61295=CARTESIAN_POINT ( 'NONE',  ( 19.60162835767302880, 5.811842276320244416, -1.500000000000002220 ) ) ;
#61298=VERTEX_POINT ( 'NONE', #74780 ) ;
#61299=ORIENTED_EDGE ( 'NONE', *, *, #29248, .T. ) ;
#61300=CARTESIAN_POINT ( 'NONE',  ( -23.06710473063640165, 0.7821689226722955413, 11.49999999999998934 ) ) ;
#61301=CARTESIAN_POINT ( 'NONE',  ( -40.11925438608624717, -25.18341647909762315, 3.283321612209681994 ) ) ;
#61302=CARTESIAN_POINT ( 'NONE',  ( -19.72078065558051208, -4.686549088087978099, -1.500000000000002220 ) ) ;
#61303=VERTEX_POINT ( 'NONE', #97131 ) ;
#61304=CARTESIAN_POINT ( 'NONE',  ( -122.5228709571500616, -24.64898659630368272, 1.056161002820833028 ) ) ;
#61307=EDGE_CURVE ( 'NONE', #64861, #6511, #91502, .T. ) ;
#61309=CARTESIAN_POINT ( 'NONE',  ( -99.51916323793128072, -23.73791477778911840, 11.05961554403170588 ) ) ;
#61310=CARTESIAN_POINT ( 'NONE',  ( 7.480126432006339421, -20.11416664461015458, 11.49999999999999645 ) ) ;
#61311=VERTEX_POINT ( 'NONE', #44356 ) ;
#61313=CARTESIAN_POINT ( 'NONE',  ( -61.65509961064937272, -23.48786465467240703, 11.44779295918255180 ) ) ;
#61314=ORIENTED_EDGE ( 'NONE', *, *, #77301, .F. ) ;
#61315=CARTESIAN_POINT ( 'NONE',  ( -4.968023186724614959, -20.10795263665959709, -1.500000000000002220 ) ) ;
#61316=ADVANCED_FACE ( 'NONE', ( #14375 ), #6274, .T. ) ;
#61317=EDGE_LOOP ( 'NONE', ( #42252, #65927, #6289, #1039 ) ) ;
#61318=CARTESIAN_POINT ( 'NONE',  ( -123.6228709571500559, -24.51283580621365132, 0.6167428607019813658 ) ) ;
#61319=ORIENTED_EDGE ( 'NONE', *, *, #9351, .F. ) ;
#61321=DIRECTION ( 'NONE',  ( -3.773278334453080206E-23, 0.9999999999976377785, 2.173523156925979975E-06 ) ) ;
#61322=ORIENTED_EDGE ( 'NONE', *, *, #3045, .T. ) ;
#61326=CARTESIAN_POINT ( 'NONE',  ( -65.62370077586832906, -25.00158670708910691, 2.256160236439222366 ) ) ;
#61327=CARTESIAN_POINT ( 'NONE',  ( 9.922928194174257754, 19.57116106031148561, 11.49999999999999645 ) ) ;
#61329=CARTESIAN_POINT ( 'NONE',  ( 19.01167203989450982, 12.12494712425435850, 11.49999999999998934 ) ) ;
#61330=CARTESIAN_POINT ( 'NONE',  ( -8.441512789788195192, 19.21024974253229800, 11.49999999999998934 ) ) ;
#61334=ORIENTED_EDGE ( 'NONE', *, *, #17923, .T. ) ;
#61335=ORIENTED_EDGE ( 'NONE', *, *, #27502, .F. ) ;
#61336=PLANE ( 'NONE',  #15826 ) ;
#61337=EDGE_CURVE ( 'NONE', #17515, #29214, #12252, .T. ) ;
#61339=CARTESIAN_POINT ( 'NONE',  ( 2.436486579176012413, 21.40072447632485364, -1.500000000000002220 ) ) ;
#61340=LINE ( 'NONE', #92759, #32775 ) ;
#61342=CARTESIAN_POINT ( 'NONE',  ( -20.44436638909326120, 5.324712401148210539, -1.500000000000002220 ) ) ;
#61344=CARTESIAN_POINT ( 'NONE',  ( -64.62739518140152484, -24.51314013834315730, 0.6176544820404094027 ) ) ;
#61345=CARTESIAN_POINT ( 'NONE',  ( -44.52287095715007581, -24.66019654487199730, 8.947790411086117501 ) ) ;
#61348=CARTESIAN_POINT ( 'NONE',  ( 8.970247382295582383, 20.24485829007567617, -1.500000000000002220 ) ) ;
#61349=CARTESIAN_POINT ( 'NONE',  ( -71.54956710204380954, -24.15543982623907127, -0.2315651400026636497 ) ) ;
#61350=ORIENTED_EDGE ( 'NONE', *, *, #38707, .T. ) ;
#61352=LINE ( 'NONE', #92773, #16776 ) ;
#61353=DIRECTION ( 'NONE',  ( 0.000000000000000000, -2.173523156925980399E-06, 0.9999999999976378895 ) ) ;
#61354=ADVANCED_FACE ( 'NONE', ( #1168 ), #31102, .T. ) ;
#61356=CARTESIAN_POINT ( 'NONE',  ( -100.5869819392765123, -24.73486907724917572, 1.287355809206965240 ) ) ;
#61357=B_SPLINE_CURVE_WITH_KNOTS ( 'NONE', 3,
 ( #14163, #28902, #45140, #61865 ),
 .UNSPECIFIED., .F., .F.,
 ( 4, 4 ),
 ( 0.000000000000000000, 9.999999999998897304E-05 ),
 .UNSPECIFIED. ) ;
#61358=CARTESIAN_POINT ( 'NONE',  ( -17.22176335520693158, -9.073154711715998744, 11.49999999999998934 ) ) ;
#61359=CARTESIAN_POINT ( 'NONE',  ( -7.638042729800005759, 19.97414216180626667, 11.49999999999998934 ) ) ;
#61360=CARTESIAN_POINT ( 'NONE',  ( -119.4728709571500360, -25.30558663486607429, 5.000950657679038791 ) ) ;
#61361=CARTESIAN_POINT ( 'NONE',  ( -105.5228709571500758, -25.00182538069145366, 7.747789668545101094 ) ) ;
#61362=CARTESIAN_POINT ( 'NONE',  ( -106.5562042904834072, -24.65952944569305316, 1.056160979905704789 ) ) ;
#61363=CARTESIAN_POINT ( 'NONE',  ( -38.62287095715005592, -24.65952944569303895, 1.056160979905692798 ) ) ;
#61364=CARTESIAN_POINT ( 'NONE',  ( -16.57510365746454184, 15.48777146884464884, -1.500000000000002220 ) ) ;
#61365=B_SPLINE_SURFACE_WITH_KNOTS ( 'NONE', 3, 3, ( 
 ( #96033, #57493, #66114, #64619 ),
 ( #18408, #81308, #12779, #11791 ),
 ( #49377, #97523, #88928, #27529 ),
 ( #34642, #10799, #41764, #19894 ),
 ( #2696, #74199, #50371, #42761 ),
 ( #88427, #73696, #58979, #72708 ),
 ( #33639, #26017, #80812, #50867 ) ),
 .UNSPECIFIED., .F., .F., .F.,
 ( 4, 3, 4 ),
 ( 4, 4 ),
 ( 0.0004766839783816396374, 0.1029713700210894006, 0.2054660560637971700 ),
 ( 0.6196516260353998051, 0.6209502567131185424 ),
 .UNSPECIFIED. ) ;
#61368=CARTESIAN_POINT ( 'NONE',  ( -7.013475202606065828, -18.52788797337992222, 11.49999999999999645 ) ) ;
#61369=LINE ( 'NONE', #38015, #20441 ) ;
#61370=EDGE_CURVE ( 'NONE', #48067, #60922, #40133, .T. ) ;
#61371=ORIENTED_EDGE ( 'NONE', *, *, #30452, .T. ) ;
#61373=CARTESIAN_POINT ( 'NONE',  ( -61.64687923781919920, -25.16711686381824364, 3.101159594853581503 ) ) ;
#61374=CARTESIAN_POINT ( 'NONE',  ( 9.069627533930374241, 19.64968329815391712, -1.500000000000002220 ) ) ;
#61375=CARTESIAN_POINT ( 'NONE',  ( -63.62287095715004881, -29.50248528299804818, 1.056150453629034924 ) ) ;
#61377=CARTESIAN_POINT ( 'NONE',  ( 19.29218144733592055, -2.436590042558338443, -1.500000000000002220 ) ) ;
#61379=FACE_OUTER_BOUND ( 'NONE', #11509, .T. ) ;
#61380=CARTESIAN_POINT ( 'NONE',  ( -4.105667982141768313, -19.37954422259287668, -1.500000000000002220 ) ) ;
#61381=ORIENTED_EDGE ( 'NONE', *, *, #7100, .F. ) ;
#61382=CARTESIAN_POINT ( 'NONE',  ( 8.409737122318338365, 18.51778827956368190, 11.49999999999999645 ) ) ;
#61383=DIRECTION ( 'NONE',  ( -3.773278334453079618E-23, 0.9999999999976377785, 2.173523156925979975E-06 ) ) ;
#61384=ADVANCED_FACE ( 'NONE', ( #63077 ), #77267, .T. ) ;
#61385=CARTESIAN_POINT ( 'NONE',  ( -46.62287095715004881, -24.66019654487198665, 8.947790411086135265 ) ) ;
#61386=ADVANCED_FACE ( 'NONE', ( #46336 ), #92996, .F. ) ;
#61387=B_SPLINE_CURVE_WITH_KNOTS ( 'NONE', 3,
 ( #82677, #64994, #3577, #34519 ),
 .UNSPECIFIED., .F., .F.,
 ( 4, 4 ),
 ( 0.000000000000000000, 9.999999999999592548E-05 ),
 .UNSPECIFIED. ) ;
#61388=ORIENTED_EDGE ( 'NONE', *, *, #20116, .F. ) ;
#61389=CARTESIAN_POINT ( 'NONE',  ( -0.04929185891187171792, -22.41187815084102652, 8.907023374642855984 ) ) ;
#61391=CARTESIAN_POINT ( 'NONE',  ( -49.08163135806235289, -25.25214541495745380, 5.465038328920414301 ) ) ;
#61392=AXIS2_PLACEMENT_3D ( 'NONE', #52648, #28309, #68869 ) ;
#61393=CARTESIAN_POINT ( 'NONE',  ( -127.6228709571500559, -24.65952944569305316, 1.056160979905707897 ) ) ;
#61394=CARTESIAN_POINT ( 'NONE',  ( -82.22287095715005023, -23.47596703998600276, 11.44779298504227683 ) ) ;
#61395=CARTESIAN_POINT ( 'NONE',  ( -16.95507112718987486, -10.73317591066004084, -1.500000000000002220 ) ) ;
#61396=EDGE_CURVE ( 'NONE', #88472, #80402, #87390, .T. ) ;
#61397=CARTESIAN_POINT ( 'NONE',  ( -120.5228709571500900, -25.00182538069145366, 7.747789668545101982 ) ) ;
#61398=ORIENTED_EDGE ( 'NONE', *, *, #11213, .T. ) ;
#61400=EDGE_CURVE ( 'NONE', #77615, #3631, #70172, .T. ) ;
#61401=CARTESIAN_POINT ( 'NONE',  ( 7.980177114813061579, 21.45908683785374649, 11.49999999999999645 ) ) ;
#61402=CARTESIAN_POINT ( 'NONE',  ( -19.63924127562733446, 11.44998032699685631, 11.49999999999998934 ) ) ;
#61403=CARTESIAN_POINT ( 'NONE',  ( -49.68676680831369197, -25.26258819900877484, 4.434853480562869876 ) ) ;
#61404=CARTESIAN_POINT ( 'NONE',  ( -126.5228709571500900, -24.51387760970726504, 9.387446482453400520 ) ) ;
#61405=CARTESIAN_POINT ( 'NONE',  ( -38.59384448668303946, -24.15620529776627379, 10.23563542870660825 ) ) ;
#61407=CARTESIAN_POINT ( 'NONE',  ( -128.5215767096398451, -24.35071581493544102, 9.817618358456019934 ) ) ;
#61408=AXIS2_PLACEMENT_3D ( 'NONE', #82940, #75329, #14426 ) ;
#61410=ORIENTED_EDGE ( 'NONE', *, *, #40565, .T. ) ;
#61411=CARTESIAN_POINT ( 'NONE',  ( 6.737473828552405841, -19.20966278261563076, 11.49999999999998934 ) ) ;
#61412=ORIENTED_EDGE ( 'NONE', *, *, #19293, .F. ) ;
#61413=CARTESIAN_POINT ( 'NONE',  ( -12.06219892284564388, 19.56905390912838172, 11.49999999999998934 ) ) ;
#61415=ORIENTED_EDGE ( 'NONE', *, *, #87362, .T. ) ;
#61416=DIRECTION ( 'NONE',  ( -3.773278334453079030E-23, 0.9999999999976377785, 2.173523156925979128E-06 ) ) ;
#61417=CARTESIAN_POINT ( 'NONE',  ( -77.51696115879298077, -23.73791477778911840, 11.05961554403170588 ) ) ;
#61418=EDGE_CURVE ( 'NONE', #48372, #89948, #3841, .T. ) ;
#61419=CARTESIAN_POINT ( 'NONE',  ( -51.61380951771659653, -23.48786465467241413, 11.44779295918254824 ) ) ;
#61420=CARTESIAN_POINT ( 'NONE',  ( -16.85803360905838488, 12.98640638483674259, 11.49999999999999645 ) ) ;
#61423=CARTESIAN_POINT ( 'NONE',  ( -0.9571703918902072505, -22.19477237104690914, -1.500000000000002220 ) ) ;
#61424=B_SPLINE_CURVE_WITH_KNOTS ( 'NONE', 3,
 ( #79956, #96192, #49529, #26680 ),
 .UNSPECIFIED., .F., .F.,
 ( 4, 4 ),
 ( 0.000000000000000000, 9.999999999998897304E-05 ),
 .UNSPECIFIED. ) ;
#61425=CARTESIAN_POINT ( 'NONE',  ( 0.06016934085327452914, 20.63536315578604174, -1.500000000000002220 ) ) ;
#61426=ORIENTED_EDGE ( 'NONE', *, *, #74682, .T. ) ;
#61427=VERTEX_POINT ( 'NONE', #14875 ) ;
#61428=CARTESIAN_POINT ( 'NONE',  ( -109.0556427821970260, -25.31627237126944152, 4.716568607272451530 ) ) ;
#61429=CARTESIAN_POINT ( 'NONE',  ( -121.6228709571500843, -24.34917612406838927, 0.1852690917426690620 ) ) ;
#61430=ORIENTED_EDGE ( 'NONE', *, *, #1607, .F. ) ;
#61433=VECTOR ( 'NONE', #3754, 1000.000000000000114 ) ;
#61435=CARTESIAN_POINT ( 'NONE',  ( -127.4728709571500360, -25.30558663486607429, 5.000950657679038791 ) ) ;
#61436=CARTESIAN_POINT ( 'NONE',  ( -44.52287095715006160, -24.64898659630367916, 1.056161002820819261 ) ) ;
#61437=CARTESIAN_POINT ( 'NONE',  ( -11.07951500695464553, -17.62175104703424466, -1.500000000000002220 ) ) ;
#61438=CARTESIAN_POINT ( 'NONE',  ( 21.63681353182189682, 2.665401433100548889, 11.49999999999999645 ) ) ;
#61439=DIRECTION ( 'NONE',  ( -3.773278334444167608E-23, 1.000000000000000000, 0.000000000000000000 ) ) ;
#61440=CARTESIAN_POINT ( 'NONE',  ( -100.4498239493576648, -25.03284467579916495, 7.563174216508126158 ) ) ;
#61441=CARTESIAN_POINT ( 'NONE',  ( 21.67916507323446496, -5.852930566066080864, 11.49999999999998934 ) ) ;
#61444=EDGE_LOOP ( 'NONE', ( #467, #49069, #36556, #84861 ) ) ;
#61445=CARTESIAN_POINT ( 'NONE',  ( -58.52287095715004739, -23.48783264082477018, -1.443836473390092801 ) ) ;
#61446=DIRECTION ( 'NONE',  ( 1.000000000000000000, 3.773278334444166432E-23, 8.201307841325785021E-29 ) ) ;
#61449=EDGE_LOOP ( 'NONE', ( #97099, #21511, #75576, #64851 ) ) ;
#61451=EDGE_CURVE ( 'NONE', #8232, #93778, #94572, .T. ) ;
#61452=CARTESIAN_POINT ( 'NONE',  ( -14.61619677566029729, 15.53698580111986693, -1.500000000000002220 ) ) ;
#61453=ORIENTED_EDGE ( 'NONE', *, *, #30644, .T. ) ;
#61454=CARTESIAN_POINT ( 'NONE',  ( 11.68726034403320746, 17.49698133428071145, 11.49999999999998934 ) ) ;
#61455=CARTESIAN_POINT ( 'NONE',  ( -30.40788910079855256, -25.13731019820412982, 2.712646531854225440 ) ) ;
#61457=CARTESIAN_POINT ( 'NONE',  ( -110.6746315611901963, -25.20166100307829993, 3.341187069408153132 ) ) ;
#61459=CARTESIAN_POINT ( 'NONE',  ( -6.321128248299066499, 21.05883132939252533, -1.500000000000002220 ) ) ;
#61460=CARTESIAN_POINT ( 'NONE',  ( -87.50252558622028687, -24.65952944569304606, 1.056160979905703678 ) ) ;
#61462=CARTESIAN_POINT ( 'NONE',  ( -80.88924702628075636, -25.30869131066464561, 4.592921213095906730 ) ) ;
#61463=ADVANCED_FACE ( 'NONE', ( #30606 ), #78265, .T. ) ;
#61464=CARTESIAN_POINT ( 'NONE',  ( -107.5562042904834215, -23.47593901973091235, -1.443836447538999312 ) ) ;
#61465=ADVANCED_FACE ( 'NONE', ( #2677 ), #65592, .T. ) ;
#61466=ADVANCED_FACE ( 'NONE', ( #79278 ), #66081, .T. ) ;
#61467=FACE_OUTER_BOUND ( 'NONE', #94878, .T. ) ;
#61468=CARTESIAN_POINT ( 'NONE',  ( -55.52287095715005449, -29.50248789122583659, 2.256150453626215580 ) ) ;
#61469=ADVANCED_FACE ( 'NONE', ( #80287 ), #83086, .T. ) ;
#61470=CARTESIAN_POINT ( 'NONE',  ( -0.08805446101867206443, -21.91006580534973480, 9.960784317162939772 ) ) ;
#61471=CARTESIAN_POINT ( 'NONE',  ( 1.764508054474889009, 21.21474994468914943, 11.49999999999998934 ) ) ;
#61472=CARTESIAN_POINT ( 'NONE',  ( -46.58953762381672448, -23.48786465467241058, 11.44779295918255180 ) ) ;
#61473=CARTESIAN_POINT ( 'NONE',  ( -107.5129983477871320, -24.51419770103159124, 9.386484678747168076 ) ) ;
#61474=CARTESIAN_POINT ( 'NONE',  ( -90.62287095715009855, -24.82558206586143967, 1.605769216559451484 ) ) ;
#61475=CARTESIAN_POINT ( 'NONE',  ( -33.47775787355578103, -24.65952944569304606, 1.056160979905695907 ) ) ;
#61476=CARTESIAN_POINT ( 'NONE',  ( -6.671648801611133273, 21.52854475820963032, -1.500000000000002220 ) ) ;
#61478=EDGE_LOOP ( 'NONE', ( #44297, #82596, #68286, #64746 ) ) ;
#61479=CARTESIAN_POINT ( 'NONE',  ( -99.10931216887415474, -25.17291523371832440, 6.862075660167399782 ) ) ;
#61480=CARTESIAN_POINT ( 'NONE',  ( 18.74904333037421011, -5.873301551693434597, 11.49999999999999645 ) ) ;
#61482=PLANE ( 'NONE',  #51252 ) ;
#61483=B_SPLINE_CURVE_WITH_KNOTS ( 'NONE', 3,
 ( #73865, #80100, #1491, #56787 ),
 .UNSPECIFIED., .F., .F.,
 ( 4, 4 ),
 ( 0.000000000000000000, 0.0001000000000000444977 ),
 .UNSPECIFIED. ) ;
#61484=ADVANCED_FACE ( 'NONE', ( #5653 ), #58465, .F. ) ;
#61486=CARTESIAN_POINT ( 'NONE',  ( -69.92726831997306647, -25.30507734521815522, 4.890125790641020487 ) ) ;
#61488=CARTESIAN_POINT ( 'NONE',  ( -100.5515626640960960, -25.31439534661152280, 5.205058145584142260 ) ) ;
#61489=CARTESIAN_POINT ( 'NONE',  ( -14.12090166725071327, 13.77431136191591143, -1.500000000000002220 ) ) ;
#61490=EDGE_CURVE ( 'NONE', #78152, #94223, #26829, .T. ) ;
#61491=ORIENTED_EDGE ( 'NONE', *, *, #31847, .T. ) ;
#61492=CARTESIAN_POINT ( 'NONE',  ( -110.0886599897713012, -25.19857471502731272, 3.319100349969234642 ) ) ;
#61493=CARTESIAN_POINT ( 'NONE',  ( -118.5228709571501184, -24.34917612406837861, 0.1852690917426619288 ) ) ;
#61496=ORIENTED_EDGE ( 'NONE', *, *, #24095, .T. ) ;
#61498=PLANE ( 'NONE',  #2105 ) ;
#61501=CARTESIAN_POINT ( 'NONE',  ( -100.6814946224345846, -29.50249428492551829, 5.197779886230994073 ) ) ;
#61505=CARTESIAN_POINT ( 'NONE',  ( 4.555139465550277933, 19.45931829295258453, 11.49999999999998934 ) ) ;
#61506=B_SPLINE_CURVE_WITH_KNOTS ( 'NONE', 3,
 ( #86428, #47373, #25022, #55488 ),
 .UNSPECIFIED., .F., .F.,
 ( 4, 4 ),
 ( 0.000000000000000000, 0.0001000000000000028644 ),
 .UNSPECIFIED. ) ;
#61508=CARTESIAN_POINT ( 'NONE',  ( -127.6228709571500559, -23.47593901973091235, -1.443836447538995760 ) ) ;
#61509=CARTESIAN_POINT ( 'NONE',  ( -45.62627668582059215, -24.92592662359561118, 8.075495903018000021 ) ) ;
#61513=VECTOR ( 'NONE', #12488, 1000.000000000000114 ) ;
#61514=CARTESIAN_POINT ( 'NONE',  ( -106.9228709571500673, -23.47593901973090169, -1.443836447538996426 ) ) ;
#61515=CARTESIAN_POINT ( 'NONE',  ( -39.62287095715005592, -29.50247984919015209, -1.443849546365060466 ) ) ;
#61516=DIRECTION ( 'NONE',  ( 0.000000000000000000, -2.173523156925979552E-06, 0.9999999999976378895 ) ) ;
#61517=CARTESIAN_POINT ( 'NONE',  ( -100.5228709571501042, -23.85229601348996553, 10.88205029486208453 ) ) ;
#61518=AXIS2_PLACEMENT_3D ( 'NONE', #92333, #76598, #29936 ) ;
#61519=B_SPLINE_CURVE_WITH_KNOTS ( 'NONE', 3,
 ( #84597, #15579, #24196, #92206, #22184, #62279 ),
 .UNSPECIFIED., .F., .F.,
 ( 4, 2, 4 ),
 ( 1.958437160922047748E-11, 0.002593568795227694981, 0.005187137570871018510 ),
 .UNSPECIFIED. ) ;
#61522=B_SPLINE_CURVE_WITH_KNOTS ( 'NONE', 3,
 ( #10863, #26591, #9853, #11360, #26081, #25071 ),
 .UNSPECIFIED., .F., .F.,
 ( 4, 2, 4 ),
 ( 6.391158118966174708E-06, 0.001387004593080789615, 0.002767618028042612838 ),
 .UNSPECIFIED. ) ;
#61525=CARTESIAN_POINT ( 'NONE',  ( -63.52287095715006160, -24.64898659630367561, 1.056161002820822592 ) ) ;
#61526=ORIENTED_EDGE ( 'NONE', *, *, #68857, .F. ) ;
#61528=CARTESIAN_POINT ( 'NONE',  ( -15.58492919356500650, -12.95507736684500699, -1.500000000000002220 ) ) ;
#61529=CARTESIAN_POINT ( 'NONE',  ( -76.62287095715009855, -24.35013146730204170, 9.818937971375111928 ) ) ;
#61533=FACE_OUTER_BOUND ( 'NONE', #48719, .T. ) ;
#61534=B_SPLINE_CURVE_WITH_KNOTS ( 'NONE', 3,
 ( #9320, #41801, #18441, #11333, #32663, #56525 ),
 .UNSPECIFIED., .F., .F.,
 ( 4, 2, 4 ),
 ( 0.000000000000000000, 0.001380901958385394833, 0.002761803916770789666 ),
 .UNSPECIFIED. ) ;
#61535=CARTESIAN_POINT ( 'NONE',  ( 16.24926901856429140, 11.90123039513101411, -1.500000000000002220 ) ) ;
#61536=CARTESIAN_POINT ( 'NONE',  ( 19.72786461798894209, 7.474574171381012100, 11.49999999999999645 ) ) ;
#61537=CARTESIAN_POINT ( 'NONE',  ( -123.6228709571500559, -29.50250243563736774, 8.947779886222134493 ) ) ;
#61538=CARTESIAN_POINT ( 'NONE',  ( 10.71795340210964120, -19.33932934982082585, 11.49999999999998934 ) ) ;
#61539=CARTESIAN_POINT ( 'NONE',  ( 7.506095096478735407, 19.11734572241606145, 11.49999999999998934 ) ) ;
#61541=CARTESIAN_POINT ( 'NONE',  ( -60.63371511099986577, -24.63355581998385446, 0.9682620441943891043 ) ) ;
#61543=FACE_OUTER_BOUND ( 'NONE', #63946, .T. ) ;
#61544=ORIENTED_EDGE ( 'NONE', *, *, #35178, .F. ) ;
#61545=PLANE ( 'NONE',  #91580 ) ;
#61548=VERTEX_POINT ( 'NONE', #66594 ) ;
#61549=EDGE_LOOP ( 'NONE', ( #84134, #32076, #88461, #83654 ) ) ;
#61550=ORIENTED_EDGE ( 'NONE', *, *, #20550, .F. ) ;
#61552=CARTESIAN_POINT ( 'NONE',  ( -75.62287095715004170, -24.99132157543084176, 2.256160258750667502 ) ) ;
#61554=CARTESIAN_POINT ( 'NONE',  ( -20.26430336558559020, 4.098603726722801710, -1.500000000000002220 ) ) ;
#61555=CARTESIAN_POINT ( 'NONE',  ( 0.9236959384754221958, 21.56878955078795812, 11.49999999999999645 ) ) ;
#61557=CARTESIAN_POINT ( 'NONE',  ( -83.62287095715005592, -23.47593901973091235, -1.443836447539004642 ) ) ;
#61559=CARTESIAN_POINT ( 'NONE',  ( -13.11617634606977489, 18.14055439154125438, 11.49999999999998934 ) ) ;
#61560=B_SPLINE_CURVE_WITH_KNOTS ( 'NONE', 3,
 ( #66624, #58995, #52370, #98024, #74694, #28522 ),
 .UNSPECIFIED., .F., .F.,
 ( 4, 2, 4 ),
 ( 6.384118678617502043E-06, 0.001386860460828380839, 0.002767336802978144494 ),
 .UNSPECIFIED. ) ;
#61563=VERTEX_POINT ( 'NONE', #83276 ) ;
#61564=CARTESIAN_POINT ( 'NONE',  ( -106.6228709571500559, -29.50250786944525672, 11.44777988621622988 ) ) ;
#61565=CARTESIAN_POINT ( 'NONE',  ( -56.52287095715006870, -29.50247984919015209, -1.443849546365056913 ) ) ;
#61567=CARTESIAN_POINT ( 'NONE',  ( -17.98194200498208062, 10.70670730041394947, 11.49999999999998934 ) ) ;
#61568=VERTEX_POINT ( 'NONE', #13754 ) ;
#61570=DIRECTION ( 'NONE',  ( -3.773278334453079030E-23, 0.9999999999976377785, 2.173523156925979128E-06 ) ) ;
#61571=ORIENTED_EDGE ( 'NONE', *, *, #58491, .F. ) ;
#61572=PLANE ( 'NONE',  #76231 ) ;
#61573=CARTESIAN_POINT ( 'NONE',  ( 20.83148622972472808, -3.941400823363257366, -1.500000000000002220 ) ) ;
#61575=CARTESIAN_POINT ( 'NONE',  ( -117.5903100292338621, -24.15543982623907837, -0.2315651400026547124 ) ) ;
#61577=EDGE_CURVE ( 'NONE', #52051, #42367, #53423, .T. ) ;
#61578=CARTESIAN_POINT ( 'NONE',  ( -16.40380107638378604, 14.33077157581830008, 11.49999999999998934 ) ) ;
#61579=CARTESIAN_POINT ( 'NONE',  ( -66.62287095715005592, -29.50250243563736774, 8.947779886222143375 ) ) ;
#61580=AXIS2_PLACEMENT_3D ( 'NONE', #46309, #15846, #14346 ) ;
#61582=CARTESIAN_POINT ( 'NONE',  ( -76.60093289846236075, -23.73791477778911840, 11.05961554403170766 ) ) ;
#61583=DIRECTION ( 'NONE',  ( -3.773278334453080206E-23, 0.9999999999976377785, 2.173523156925979975E-06 ) ) ;
#61584=CARTESIAN_POINT ( 'NONE',  ( -18.37375256118794553, 11.78967355450649457, -1.500000000000002220 ) ) ;
#61588=CARTESIAN_POINT ( 'NONE',  ( -123.6228709571500559, -24.65952944569304961, 1.056160979905703234 ) ) ;
#61590=ORIENTED_EDGE ( 'NONE', *, *, #68134, .F. ) ;
#61592=VECTOR ( 'NONE', #60092, 1000.000000000000114 ) ;
#61593=EDGE_CURVE ( 'NONE', #65225, #48372, #95840, .T. ) ;
#61594=VERTEX_POINT ( 'NONE', #29481 ) ;
#61595=ADVANCED_FACE ( 'NONE', ( #91384 ), #50347, .F. ) ;
#61596=AXIS2_PLACEMENT_3D ( 'NONE', #82248, #41715, #95981 ) ;
#61600=CARTESIAN_POINT ( 'NONE',  ( -13.45780860896912934, -16.40347334334247265, -1.500000000000002220 ) ) ;
#61602=CARTESIAN_POINT ( 'NONE',  ( -79.79245360944284471, -25.27791940355850286, 7.413204867740626369 ) ) ;
#61603=DIRECTION ( 'NONE',  ( 0.000000000000000000, -0.9999999999976377785, -2.173523156925979128E-06 ) ) ;
#61605=CARTESIAN_POINT ( 'NONE',  ( -9.899997732206244905, -16.63842163800745766, -1.500000000000002220 ) ) ;
#61606=CARTESIAN_POINT ( 'NONE',  ( -69.86753664201866343, -25.30877541009007459, 5.411526165084938889 ) ) ;
#61607=EDGE_LOOP ( 'NONE', ( #3472, #44446, #55214, #26517 ) ) ;
#61608=CARTESIAN_POINT ( 'NONE',  ( -19.06185424839875964, 3.971334347869299286, 11.49999999999999645 ) ) ;
#61609=CARTESIAN_POINT ( 'NONE',  ( -34.52287095715006160, -23.48783264083359867, -1.443836473376372442 ) ) ;
#61610=CARTESIAN_POINT ( 'NONE',  ( -49.62287095715005592, -24.64965695001467694, 8.947790433994185832 ) ) ;
#61612=ORIENTED_EDGE ( 'NONE', *, *, #91451, .T. ) ;
#61613=DIRECTION ( 'NONE',  ( 1.000000000000000000, 3.773278334444167608E-23, 8.201307833595939069E-29 ) ) ;
#61614=PLANE ( 'NONE',  #38458 ) ;
#61615=CARTESIAN_POINT ( 'NONE',  ( -45.62287095715004881, -25.00158670708908915, 2.256160236439166855 ) ) ;
#61617=CARTESIAN_POINT ( 'NONE',  ( -17.63651738508609412, 8.604534254076446231, -1.500000000000002220 ) ) ;
#61618=EDGE_CURVE ( 'NONE', #60030, #26877, #98156, .T. ) ;
#61619=DIRECTION ( 'NONE',  ( 0.000000000000000000, -2.173523156925979552E-06, 0.9999999999976378895 ) ) ;
#61620=ORIENTED_EDGE ( 'NONE', *, *, #81316, .F. ) ;
#61621=CARTESIAN_POINT ( 'NONE',  ( 14.45009471711328786, 16.04676183837579373, -1.500000000000002220 ) ) ;
#61622=CARTESIAN_POINT ( 'NONE',  ( -95.52287095715006160, -23.48786465467241769, 11.44779295918254114 ) ) ;
#61623=CARTESIAN_POINT ( 'NONE',  ( -78.94303308397306296, -29.50249597972496929, 5.977527482382998691 ) ) ;
#61624=FACE_OUTER_BOUND ( 'NONE', #30598, .T. ) ;
#61625=CARTESIAN_POINT ( 'NONE',  ( -11.53412672884717871, -19.92380006517282709, -1.500000000000002220 ) ) ;
#61627=CARTESIAN_POINT ( 'NONE',  ( -75.62287095715005592, -23.47593901973091235, -1.443836447539004642 ) ) ;
#61629=CARTESIAN_POINT ( 'NONE',  ( -121.5192058621623090, -24.35071581493543746, 9.817618358456025263 ) ) ;
#61630=CARTESIAN_POINT ( 'NONE',  ( -101.5351826556731254, -25.12726549548206023, 7.135831474093189186 ) ) ;
#61631=CARTESIAN_POINT ( 'NONE',  ( -109.3900273060415316, -25.26106641928794971, 3.961258450193692493 ) ) ;
#61632=CARTESIAN_POINT ( 'NONE',  ( -129.5219158117283769, -24.34968618360934300, 0.1864209137778921610 ) ) ;
#61633=CARTESIAN_POINT ( 'NONE',  ( -99.60745734687597519, -25.26400877198413042, 4.898549832726014408 ) ) ;
#61634=CARTESIAN_POINT ( 'NONE',  ( 19.12242951303546334, 5.485007674754557527, -1.500000000000002220 ) ) ;
#61636=CARTESIAN_POINT ( 'NONE',  ( 19.75791096855702733, 1.210928449428283038, -1.500000000000002220 ) ) ;
#61637=CARTESIAN_POINT ( 'NONE',  ( -56.62367352497894757, -24.65952944569304250, 1.056160979905696795 ) ) ;
#61638=ADVANCED_FACE ( 'NONE', ( #66093 ), #51842, .T. ) ;
#61639=CARTESIAN_POINT ( 'NONE',  ( -39.14342005660770241, -25.29116703577911807, 3.683763317769410683 ) ) ;
#61640=DIRECTION ( 'NONE',  ( -3.773278334453079618E-23, 0.9999999999976377785, 2.173523156925979975E-06 ) ) ;
#61641=CARTESIAN_POINT ( 'NONE',  ( 17.59156710592704442, 10.99281682905060897, 11.49999999999999645 ) ) ;
#61642=PLANE ( 'NONE',  #12700 ) ;
#61644=ADVANCED_FACE ( 'NONE', ( #97990 ), #75163, .F. ) ;
#61646=CARTESIAN_POINT ( 'NONE',  ( -22.07869367785253090, -5.390224856484156390, 11.49999999999999645 ) ) ;
#61649=CARTESIAN_POINT ( 'NONE',  ( -28.52287095715005805, -24.49893655963190042, 1.056161680022248195 ) ) ;
#61650=CARTESIAN_POINT ( 'NONE',  ( 19.91930514195032487, 3.327535025408205893, -1.500000000000002220 ) ) ;
#61652=CARTESIAN_POINT ( 'NONE',  ( -45.62287095715005592, -23.48786465467240703, 11.44779295918255002 ) ) ;
#61656=CARTESIAN_POINT ( 'NONE',  ( 15.01570752033863165, -17.30494853738164096, -1.500000000000002220 ) ) ;
#61657=CARTESIAN_POINT ( 'NONE',  ( -41.31104052750491462, -25.16585682362166310, 3.095323067379869730 ) ) ;
#61658=VECTOR ( 'NONE', #91766, 1000.000000000000000 ) ;
#61659=CARTESIAN_POINT ( 'NONE',  ( 7.158504886898216846, -20.39052948596947346, -1.500000000000002220 ) ) ;
#61660=CARTESIAN_POINT ( 'NONE',  ( -123.5222519537087464, -23.48783264082477373, -1.443836473390086361 ) ) ;
#61661=CARTESIAN_POINT ( 'NONE',  ( -34.60964202172039705, -23.73766607897670866, -1.055555164236443133 ) ) ;
#61662=B_SPLINE_CURVE_WITH_KNOTS ( 'NONE', 3,
 ( #37310, #68257, #99185, #60656, #91578, #78344, #56040, #10347, #15946, #39291, #41301, #87472, #25062, #1247 ),
 .UNSPECIFIED., .F., .F.,
 ( 4, 2, 2, 2, 2, 2, 4 ),
 ( 0.000000000000000000, 0.0001905927013275506747, 0.0003811854026551013495, 0.0007623708053102105052, 0.001143556207965319444, 0.001334148909292864373, 0.001524741610620409084 ),
 .UNSPECIFIED. ) ;
#61663=CARTESIAN_POINT ( 'NONE',  ( 20.89859092893058801, 0.06103081833375877813, 11.49999999999999645 ) ) ;
#61664=ORIENTED_EDGE ( 'NONE', *, *, #73734, .F. ) ;
#61665=AXIS2_PLACEMENT_3D ( 'NONE', #50539, #79983, #88607 ) ;
#61666=CARTESIAN_POINT ( 'NONE',  ( -124.5909689015293367, -23.73766607897671577, -1.055555164236449572 ) ) ;
#61667=CARTESIAN_POINT ( 'NONE',  ( 2.959355296939036872, -21.81356824310248399, 11.49999999999998934 ) ) ;
#61669=CARTESIAN_POINT ( 'NONE',  ( -105.5186459176268983, -23.85049219812686871, 10.88485053497526955 ) ) ;
#61670=DIRECTION ( 'NONE',  ( -3.773278334444167608E-23, 1.000000000000000000, 0.000000000000000000 ) ) ;
#61671=ORIENTED_EDGE ( 'NONE', *, *, #57077, .T. ) ;
#61673=FACE_OUTER_BOUND ( 'NONE', #10866, .T. ) ;
#61674=ORIENTED_EDGE ( 'NONE', *, *, #4776, .F. ) ;
#61675=CARTESIAN_POINT ( 'NONE',  ( -72.58096329547595360, -24.66019654487199730, 8.947790411086121054 ) ) ;
#61679=CARTESIAN_POINT ( 'NONE',  ( -95.62287095715007013, -23.48786465467241769, 11.44779295918254114 ) ) ;
#61680=CARTESIAN_POINT ( 'NONE',  ( -36.50467997377245410, -23.96119346886880308, -0.6495511937832127991 ) ) ;
#61681=CARTESIAN_POINT ( 'NONE',  ( 19.60162835767302880, 5.811842276320244416, -1.500000000000002220 ) ) ;
#61682=ORIENTED_EDGE ( 'NONE', *, *, #94146, .F. ) ;
#61686=CARTESIAN_POINT ( 'NONE',  ( 17.40631026334068565, 13.93540124644318645, -1.500000000000002220 ) ) ;
#61688=CARTESIAN_POINT ( 'NONE',  ( -51.58953762381672448, -24.64965694238407323, 8.947790433994656567 ) ) ;
#61689=ORIENTED_EDGE ( 'NONE', *, *, #72996, .F. ) ;
#61690=CARTESIAN_POINT ( 'NONE',  ( -27.79962520430046524, -24.61258123373733753, 1.630330808770078743 ) ) ;
#61691=CARTESIAN_POINT ( 'NONE',  ( -28.41099462919338237, -25.26248047940597985, 8.118937510302929539 ) ) ;
#61692=CARTESIAN_POINT ( 'NONE',  ( 15.94631523246878579, 13.42178585792578360, -1.500000000000002220 ) ) ;
#61693=ORIENTED_EDGE ( 'NONE', *, *, #88458, .T. ) ;
#61694=CARTESIAN_POINT ( 'NONE',  ( -42.52287095715005449, -23.73934037231755667, 11.05740245334330041 ) ) ;
#61695=ORIENTED_EDGE ( 'NONE', *, *, #93777, .F. ) ;
#61697=ORIENTED_EDGE ( 'NONE', *, *, #8924, .T. ) ;
#61698=ORIENTED_EDGE ( 'NONE', *, *, #77577, .T. ) ;
#61699=DIRECTION ( 'NONE',  ( 1.000000000000000000, 3.773278334444167608E-23, 8.201307833595939069E-29 ) ) ;
#61701=ADVANCED_FACE ( 'NONE', ( #60956 ), #22854, .T. ) ;
#61702=LINE ( 'NONE', #77890, #84177 ) ;
#61703=CARTESIAN_POINT ( 'NONE',  ( -108.9952638098694990, -25.25813793666175755, 3.818317156516219502 ) ) ;
#61704=CARTESIAN_POINT ( 'NONE',  ( -53.62287095715004881, -23.48783264082478084, -1.443836473390070596 ) ) ;
#61705=CARTESIAN_POINT ( 'NONE',  ( 22.20243239366838850, -0.07139729354238147363, 11.49999999999999645 ) ) ;
#61706=ORIENTED_EDGE ( 'NONE', *, *, #91269, .F. ) ;
#61710=CARTESIAN_POINT ( 'NONE',  ( 0.4201012023153268271, 22.63755686032812164, -1.500000000000002220 ) ) ;
#61711=EDGE_CURVE ( 'NONE', #63420, #87407, #23865, .T. ) ;
#61712=CARTESIAN_POINT ( 'NONE',  ( -115.5935066442949619, -23.85049219812686871, 10.88485053497526778 ) ) ;
#61713=ORIENTED_EDGE ( 'NONE', *, *, #61849, .F. ) ;
#61714=ADVANCED_FACE ( 'NONE', ( #62961 ), #13413, .T. ) ;
#61715=VERTEX_POINT ( 'NONE', #72567 ) ;
#61716=EDGE_CURVE ( 'NONE', #34088, #14044, #13518, .T. ) ;
#61718=B_SPLINE_CURVE_WITH_KNOTS ( 'NONE', 3,
 ( #30672, #90084, #51528, #12942 ),
 .UNSPECIFIED., .F., .F.,
 ( 4, 4 ),
 ( 0.000000000000000000, 9.999999999997510880E-05 ),
 .UNSPECIFIED. ) ;
#61720=CARTESIAN_POINT ( 'NONE',  ( -15.79248070760165490, 12.47733877207048181, -1.500000000000002220 ) ) ;
#61722=EDGE_LOOP ( 'NONE', ( #75287, #83127, #95992, #84183 ) ) ;
#61723=DIRECTION ( 'NONE',  ( 0.000000000000000000, -0.9999999999976377785, -2.173523156925979128E-06 ) ) ;
#61724=CARTESIAN_POINT ( 'NONE',  ( 2.183928509170398602, -22.20744181112294413, -1.500000000000002220 ) ) ;
#61726=ORIENTED_EDGE ( 'NONE', *, *, #24452, .F. ) ;
#61728=CARTESIAN_POINT ( 'NONE',  ( -101.1944152955115044, -25.25341239125477344, 6.858245852482038885 ) ) ;
#61729=CARTESIAN_POINT ( 'NONE',  ( -119.6228709571500701, -24.50321055353803246, 9.387540953477515160 ) ) ;
#61730=CARTESIAN_POINT ( 'NONE',  ( -58.52287095715006160, -29.50250243563736774, 8.947779886222145151 ) ) ;
#61732=EDGE_CURVE ( 'NONE', #55816, #96695, #88290, .T. ) ;
#61735=CARTESIAN_POINT ( 'NONE',  ( 19.09806219120973125, -4.162641619376711510, -1.500000000000002220 ) ) ;
#61738=CARTESIAN_POINT ( 'NONE',  ( -21.47443924280258187, -0.1944818460393343829, -1.500000000000002220 ) ) ;
#61742=CARTESIAN_POINT ( 'NONE',  ( -68.62287095715011276, -23.95044443724992789, 10.65354141964649415 ) ) ;
#61743=CARTESIAN_POINT ( 'NONE',  ( 16.68310095749102118, 15.68496000196893370, -1.500000000000002220 ) ) ;
#61745=CARTESIAN_POINT ( 'NONE',  ( -91.15361000704997707, -29.50249591506787894, 5.947779886229223045 ) ) ;
#61747=CARTESIAN_POINT ( 'NONE',  ( 11.63622169266987783, 16.31392799894670631, 11.49999999999999645 ) ) ;
#61748=CARTESIAN_POINT ( 'NONE',  ( -78.94416233434603214, -25.26612682183856862, 5.924886500966431768 ) ) ;
#61749=CARTESIAN_POINT ( 'NONE',  ( -113.5228709571500616, -24.64965694238408034, 8.947790433994192938 ) ) ;
#61753=FACE_OUTER_BOUND ( 'NONE', #93634, .T. ) ;
#61755=CARTESIAN_POINT ( 'NONE',  ( -109.0885707575500447, -25.22089525921357733, 3.567658405505949482 ) ) ;
#61756=CARTESIAN_POINT ( 'NONE',  ( -21.25272785503416273, -4.502612752106283978, -1.500000000000002220 ) ) ;
#61758=CARTESIAN_POINT ( 'NONE',  ( -18.14765110722914798, -7.448729197826248871, -1.500000000000002220 ) ) ;
#61759=CARTESIAN_POINT ( 'NONE',  ( -128.5895376238167103, -24.64898659630529565, 1.056161002820832806 ) ) ;
#61760=CARTESIAN_POINT ( 'NONE',  ( -109.3602963299949806, -25.27925676388351306, 4.255031605239652848 ) ) ;
#61761=CARTESIAN_POINT ( 'NONE',  ( -91.62825878037952521, -24.35071581493543391, 9.817618358456023486 ) ) ;
#61762=CARTESIAN_POINT ( 'NONE',  ( -47.52287095715007581, -23.72773821059537269, 11.05748984161097326 ) ) ;
#61763=CARTESIAN_POINT ( 'NONE',  ( 2.947869850540926429, 20.32360706268488215, 11.49999999999999645 ) ) ;
#61765=CARTESIAN_POINT ( 'NONE',  ( -120.6235064633471268, -25.00158670708911046, 2.256160236439219258 ) ) ;
#61768=CARTESIAN_POINT ( 'NONE',  ( -46.62287095715004170, -23.48783264082478439, -1.443836473390070818 ) ) ;
#61770=CARTESIAN_POINT ( 'NONE',  ( -125.5545351961102369, -24.73531770709095312, 8.716586749053508498 ) ) ;
#61773=CARTESIAN_POINT ( 'NONE',  ( -25.59878527050454622, -24.93063146600816538, 6.005086248586695596 ) ) ;
#61775=CARTESIAN_POINT ( 'NONE',  ( 19.24196208499951055, 12.69117723712289703, 11.49999999999999645 ) ) ;
#61776=CARTESIAN_POINT ( 'NONE',  ( 2.581029390964978187, -22.66945732913600509, 11.49999999999998934 ) ) ;
#61777=CARTESIAN_POINT ( 'NONE',  ( -74.63881430719601440, -23.96119346886880308, -0.6495511937832119109 ) ) ;
#61779=CARTESIAN_POINT ( 'NONE',  ( -104.6228709571500559, -24.66019654487200086, 8.947790411086124607 ) ) ;
#61780=CARTESIAN_POINT ( 'NONE',  ( 20.53814608839396527, -8.957171556794316203, 11.49999999999999645 ) ) ;
#61782=CARTESIAN_POINT ( 'NONE',  ( -29.52287095715006870, -23.40099448348795264, -1.443836171194820883 ) ) ;
#61783=CARTESIAN_POINT ( 'NONE',  ( -43.60777470970129599, -23.73766607897671221, -1.055555164236442689 ) ) ;
#61785=CARTESIAN_POINT ( 'NONE',  ( 17.58553779993395594, 13.13030503331179411, -1.500000000000002220 ) ) ;
#61789=CARTESIAN_POINT ( 'NONE',  ( -104.5858024219328399, -24.65952944569305316, 1.056160979905702346 ) ) ;
#61790=CARTESIAN_POINT ( 'NONE',  ( -78.52212890984405647, -23.48783264082477018, -1.443836473390096797 ) ) ;
#61791=CARTESIAN_POINT ( 'NONE',  ( -91.52287095715006160, -29.50248528299804818, 1.056150453629040253 ) ) ;
#61792=ORIENTED_EDGE ( 'NONE', *, *, #16817, .F. ) ;
#61793=CARTESIAN_POINT ( 'NONE',  ( -20.16212974941129588, 3.559051167911782887, -1.500000000000002220 ) ) ;
#61798=CARTESIAN_POINT ( 'NONE',  ( 7.103900956763240515, -21.94381868531750968, 11.49999999999998934 ) ) ;
#61799=CARTESIAN_POINT ( 'NONE',  ( -82.52287095715006160, -23.72747288104470087, -1.053458166803226126 ) ) ;
#61800=CARTESIAN_POINT ( 'NONE',  ( 19.35245777310151993, -6.127589836641541332, -1.500000000000002220 ) ) ;
#61801=VERTEX_POINT ( 'NONE', #43115 ) ;
#61802=CARTESIAN_POINT ( 'NONE',  ( -79.11611000704996854, -25.14083923594767001, 2.947789366383933185 ) ) ;
#61803=CARTESIAN_POINT ( 'NONE',  ( -92.55803704003275811, -23.73766607897670866, -1.055555164236430032 ) ) ;
#61806=CARTESIAN_POINT ( 'NONE',  ( -70.58423775607164430, -24.73486907724917572, 1.287355809206963908 ) ) ;
#61807=CARTESIAN_POINT ( 'NONE',  ( 13.13055478438326773, -17.03443908202477886, 11.49999999999999645 ) ) ;
#61808=ORIENTED_EDGE ( 'NONE', *, *, #13626, .F. ) ;
#61809=DIRECTION ( 'NONE',  ( 0.000000000000000000, -2.173523156925979552E-06, 0.9999999999976378895 ) ) ;
#61810=CARTESIAN_POINT ( 'NONE',  ( -61.49888431235496000, -24.35071581493542681, 9.817618358456030592 ) ) ;
#61812=VERTEX_POINT ( 'NONE', #13139 ) ;
#61813=CARTESIAN_POINT ( 'NONE',  ( 20.56943099487245519, -2.726235779781958968, 11.49999999999998934 ) ) ;
#61814=B_SPLINE_CURVE_WITH_KNOTS ( 'NONE', 3,
 ( #30401, #61373, #45145, #7069 ),
 .UNSPECIFIED., .F., .F.,
 ( 4, 4 ),
 ( 2.818811872883924926E-06, 0.0004696340498052392208 ),
 .UNSPECIFIED. ) ;
#61816=CARTESIAN_POINT ( 'NONE',  ( -73.62287095715005592, -23.48783264082478084, -1.443836473390067487 ) ) ;
#61817=VERTEX_POINT ( 'NONE', #73563 ) ;
#61819=ORIENTED_EDGE ( 'NONE', *, *, #82634, .T. ) ;
#61820=VERTEX_POINT ( 'NONE', #90779 ) ;
#61822=FACE_OUTER_BOUND ( 'NONE', #82241, .T. ) ;
#61823=CARTESIAN_POINT ( 'NONE',  ( -124.5228709571501327, -23.96177878511309345, 10.65340807706329507 ) ) ;
#61824=CARTESIAN_POINT ( 'NONE',  ( -3.149188516569510377, 21.71089317892358395, 11.49999999999999645 ) ) ;
#61825=CARTESIAN_POINT ( 'NONE',  ( -90.62287095715002749, -25.00182538069145366, 7.747789668545099317 ) ) ;
#61826=CARTESIAN_POINT ( 'NONE',  ( 19.88857169258762170, 10.62688394266798930, 11.49999999999998934 ) ) ;
#61827=CARTESIAN_POINT ( 'NONE',  ( -2.499008156623981236, -20.81284420272260860, 11.49999999999998934 ) ) ;
#61828=CARTESIAN_POINT ( 'NONE',  ( -109.6485548560138312, -25.30376161434310234, 5.552256222609500469 ) ) ;
#61830=ORIENTED_EDGE ( 'NONE', *, *, #92509, .F. ) ;
#61832=ORIENTED_EDGE ( 'NONE', *, *, #21230, .F. ) ;
#61835=PLANE ( 'NONE',  #53100 ) ;
#61836=CARTESIAN_POINT ( 'NONE',  ( 20.53733210929814845, -6.371126427052321795, -1.500000000000002220 ) ) ;
#61837=VECTOR ( 'NONE', #30741, 1000.000000000000114 ) ;
#61840=CARTESIAN_POINT ( 'NONE',  ( 17.61891135320703938, 11.69080507458975227, -1.500000000000002220 ) ) ;
#61841=DIRECTION ( 'NONE',  ( -3.773278334453079030E-23, 0.9999999999976377785, 2.173523156925979128E-06 ) ) ;
#61842=CARTESIAN_POINT ( 'NONE',  ( -60.72894938232060724, -25.20144863547804803, 6.835696751361012957 ) ) ;
#61843=CARTESIAN_POINT ( 'NONE',  ( -83.59947989562338933, -23.73791477778912196, 11.05961554403170588 ) ) ;
#61844=FACE_OUTER_BOUND ( 'NONE', #79193, .T. ) ;
#61845=CARTESIAN_POINT ( 'NONE',  ( -47.62287095715004881, -24.50321055353803956, 9.387540953477536476 ) ) ;
#61846=CARTESIAN_POINT ( 'NONE',  ( -7.471142097702432316, -20.87072022463130239, -1.500000000000002220 ) ) ;
#61847=CARTESIAN_POINT ( 'NONE',  ( -71.54510427940205375, -24.34968618360933945, 0.1864209137778822800 ) ) ;
#61848=B_SPLINE_CURVE_WITH_KNOTS ( 'NONE', 3,
 ( #40001, #39506, #93275, #54242 ),
 .UNSPECIFIED., .F., .F.,
 ( 4, 4 ),
 ( 0.4501073351080630003, 0.4591137663801785895 ),
 .UNSPECIFIED. ) ;
#61849=EDGE_CURVE ( 'NONE', #81082, #97756, #92245, .T. ) ;
#61850=ORIENTED_EDGE ( 'NONE', *, *, #95473, .T. ) ;
#61851=CARTESIAN_POINT ( 'NONE',  ( -51.35838135674943317, -25.31633125061866352, 5.126937609008879626 ) ) ;
#61853=CARTESIAN_POINT ( 'NONE',  ( -126.5552529902581256, -24.34968618360934300, 0.1864209137778884418 ) ) ;
#61854=B_SPLINE_CURVE_WITH_KNOTS ( 'NONE', 3,
 ( #62503, #37157, #29537, #76696, #92931, #53890, #7197, #68612, #77198, #7705, #38652, #45279 ),
 .UNSPECIFIED., .F., .F.,
 ( 4, 2, 2, 2, 2, 4 ),
 ( 0.000000000000000000, 0.0001514886653422532943, 0.0003029773306845065886, 0.0006059546613690202244, 0.0009089319920535340229, 0.001211909322738047821 ),
 .UNSPECIFIED. ) ;
#61856=CARTESIAN_POINT ( 'NONE',  ( 18.80106323769845389, 4.952424739525837616, 11.49999999999998934 ) ) ;
#61857=CARTESIAN_POINT ( 'NONE',  ( -17.20161093224466953, -12.68000408521323408, -1.500000000000002220 ) ) ;
#61858=CARTESIAN_POINT ( 'NONE',  ( -38.52287095715006870, -23.48786465467241058, 11.44779295918255180 ) ) ;
#61859=CARTESIAN_POINT ( 'NONE',  ( -89.80332600318982372, -25.31973986624387862, 5.294390042787146200 ) ) ;
#61861=CARTESIAN_POINT ( 'NONE',  ( -46.62287095715004170, -23.48783264082478439, -1.443836473390070818 ) ) ;
#61863=CARTESIAN_POINT ( 'NONE',  ( -19.30582015231555104, -11.89196067722419237, -1.500000000000002220 ) ) ;
#61865=CARTESIAN_POINT ( 'NONE',  ( -97.52287095715006160, -24.64898659630367916, 1.056161002820829697 ) ) ;
#61866=CARTESIAN_POINT ( 'NONE',  ( -19.84341114293531305, -1.032944114202840824, 11.49999999999999645 ) ) ;
#61867=CARTESIAN_POINT ( 'NONE',  ( -73.62287095715005592, -23.47593901973091235, -1.443836447539006196 ) ) ;
#61868=ORIENTED_EDGE ( 'NONE', *, *, #16428, .F. ) ;
#61873=CARTESIAN_POINT ( 'NONE',  ( 8.597998336517790108, -19.88058937513707392, -1.500000000000002220 ) ) ;
#61875=CARTESIAN_POINT ( 'NONE',  ( 19.43689267596983683, 0.5339526363925560792, -1.500000000000002220 ) ) ;
#61876=CARTESIAN_POINT ( 'NONE',  ( -80.52287095715007581, -24.83620972994591014, 8.398175272781370992 ) ) ;
#61877=DIRECTION ( 'NONE',  ( -0.000000000000000000, 2.173523156925979552E-06, -0.9999999999976378895 ) ) ;
#61878=CARTESIAN_POINT ( 'NONE',  ( -9.134819693115781902, 17.59984377705169933, -1.500000000000002220 ) ) ;
#61879=EDGE_CURVE ( 'NONE', #1347, #19743, #72851, .T. ) ;
#61883=CARTESIAN_POINT ( 'NONE',  ( 16.70477854660759931, 11.60849435585976153, 11.49999999999999645 ) ) ;
#61884=CARTESIAN_POINT ( 'NONE',  ( -80.63530711448595412, -24.40034930558991277, 0.3402023900116063482 ) ) ;
#61887=VERTEX_POINT ( 'NONE', #74062 ) ;
#61888=CARTESIAN_POINT ( 'NONE',  ( -30.59755354180557418, -24.77158516743337913, 8.907023374642857760 ) ) ;
#61889=CARTESIAN_POINT ( 'NONE',  ( -119.4728709594060376, -25.21147767946275664, 8.000950760261451578 ) ) ;
#61890=CARTESIAN_POINT ( 'NONE',  ( -101.5228709571500758, -29.50248528299804818, 1.056150453629042030 ) ) ;
#61891=CARTESIAN_POINT ( 'NONE',  ( -40.53724472056929784, -24.52399227489126687, 9.353111116836521077 ) ) ;
#61892=DIRECTION ( 'NONE',  ( 0.000000000000000000, 0.9999999999976377785, 2.173523156925979975E-06 ) ) ;
#61893=CARTESIAN_POINT ( 'NONE',  ( 11.77038589110637901, 16.27938679534767275, -1.500000000000002220 ) ) ;
#61896=CARTESIAN_POINT ( 'NONE',  ( -97.26334014122947735, -23.56000036390797092, -1.497999999999530374 ) ) ;
#61897=CARTESIAN_POINT ( 'NONE',  ( -4.526818761702180893, -22.41603498850323817, 11.49999999999999645 ) ) ;
#61898=CARTESIAN_POINT ( 'NONE',  ( -13.93578158028743985, 17.96481793202167054, 11.49999999999998934 ) ) ;
#61899=VERTEX_POINT ( 'NONE', #26884 ) ;
#61900=CARTESIAN_POINT ( 'NONE',  ( -53.62287095715007013, -23.73934037231756733, 11.05740245334329153 ) ) ;
#61901=CARTESIAN_POINT ( 'NONE',  ( -53.62287095715005592, -29.50250243563736774, 8.947779886222146928 ) ) ;
#61902=CARTESIAN_POINT ( 'NONE',  ( -38.60882062815987581, -23.73791477778911485, 11.05961554403170766 ) ) ;
#61904=EDGE_CURVE ( 'NONE', #56351, #89504, #49857, .T. ) ;
#61908=CARTESIAN_POINT ( 'NONE',  ( 18.16468007720714795, -9.286844270591712913, 11.49999999999998934 ) ) ;
#61910=CARTESIAN_POINT ( 'NONE',  ( -12.06219892284564388, 19.56905390912838172, -1.500000000000002220 ) ) ;
#61911=DIRECTION ( 'NONE',  ( -3.773278334444166432E-23, 1.000000000000000000, 0.000000000000000000 ) ) ;
#61912=EDGE_CURVE ( 'NONE', #31190, #14381, #63143, .T. ) ;
#61915=CARTESIAN_POINT ( 'NONE',  ( -81.18457222299012699, -25.17491913618721355, 6.847625054176566195 ) ) ;
#61916=CARTESIAN_POINT ( 'NONE',  ( -51.51435870162961095, -23.73791477778911840, 11.05961554403170766 ) ) ;
#61917=CARTESIAN_POINT ( 'NONE',  ( 21.10678091372558640, -2.468637549841573797, 11.49999999999999645 ) ) ;
#61918=VERTEX_POINT ( 'NONE', #20254 ) ;
#61920=CARTESIAN_POINT ( 'NONE',  ( 13.39142644571787422, -17.71860720625715757, -1.500000000000002220 ) ) ;
#61922=CARTESIAN_POINT ( 'NONE',  ( -4.704028875484805639, -20.06825252194306941, -1.500000000000002220 ) ) ;
#61924=ORIENTED_EDGE ( 'NONE', *, *, #81691, .T. ) ;
#61925=CARTESIAN_POINT ( 'NONE',  ( -112.6228709571500701, -24.33927499327855415, 9.819080762295817166 ) ) ;
#61926=CARTESIAN_POINT ( 'NONE',  ( -68.92252889959623019, -25.25978459231412288, 3.590539514744167437 ) ) ;
#61927=ORIENTED_EDGE ( 'NONE', *, *, #71347, .T. ) ;
#61930=CARTESIAN_POINT ( 'NONE',  ( -49.52287095715005449, -24.50321055353802890, 9.387540953477525818 ) ) ;
#61932=PLANE ( 'NONE',  #21147 ) ;
#61933=CARTESIAN_POINT ( 'NONE',  ( 20.80141654084381386, -1.409215765453083469, -1.500000000000002220 ) ) ;
#61935=CARTESIAN_POINT ( 'NONE',  ( 1.472770742059883897, 21.73951962378590963, 11.49999999999999645 ) ) ;
#61938=CARTESIAN_POINT ( 'NONE',  ( -22.32441756149717094, -2.617931739244098388, 11.49999999999998934 ) ) ;
#61939=CARTESIAN_POINT ( 'NONE',  ( -38.61775694482038546, -23.48783264082477729, -1.443836473390076369 ) ) ;
#61941=B_SPLINE_CURVE_WITH_KNOTS ( 'NONE', 3,
 ( #13279, #75180, #73697, #11792, #27530, #19896 ),
 .UNSPECIFIED., .F., .F.,
 ( 4, 2, 4 ),
 ( 1.570887131794333942E-05, 0.001396322306279761073, 0.002776935741241578874 ),
 .UNSPECIFIED. ) ;
#61947=ORIENTED_EDGE ( 'NONE', *, *, #89084, .T. ) ;
#61948=EDGE_CURVE ( 'NONE', #77573, #39962, #36353, .T. ) ;
#61950=CARTESIAN_POINT ( 'NONE',  ( 12.02608574658498597, -17.65016651952024063, -1.500000000000002220 ) ) ;
#61951=ADVANCED_FACE ( 'NONE', ( #67954 ), #46108, .T. ) ;
#61953=CARTESIAN_POINT ( 'NONE',  ( 12.99892964944760543, 16.54660993828877125, -1.500000000000002220 ) ) ;
#61954=CARTESIAN_POINT ( 'NONE',  ( -30.53009561173929143, -23.47879756175468557, -1.443836490256471983 ) ) ;
#61955=LINE ( 'NONE', #92881, #80929 ) ;
#61956=CARTESIAN_POINT ( 'NONE',  ( -61.58953762381671737, -23.48783264082478439, -1.443836473390069042 ) ) ;
#61957=CARTESIAN_POINT ( 'NONE',  ( 12.93620265873104991, 17.78788284566447331, -1.500000000000002220 ) ) ;
#61959=ORIENTED_EDGE ( 'NONE', *, *, #31679, .T. ) ;
#61960=CARTESIAN_POINT ( 'NONE',  ( -71.30457154551152144, -29.50249648326654039, 6.209198155459374924 ) ) ;
#61961=EDGE_CURVE ( 'NONE', #35718, #34952, #83656, .T. ) ;
#61962=CARTESIAN_POINT ( 'NONE',  ( -107.5228709571501042, -23.47593901973090524, -1.443836447538996426 ) ) ;
#61963=CARTESIAN_POINT ( 'NONE',  ( -19.76906661924035191, -6.534152953431121347, 11.49999999999999645 ) ) ;
#61966=CARTESIAN_POINT ( 'NONE',  ( -108.6228709571499991, -24.51387760970724372, 9.387446482453409402 ) ) ;
#61967=CARTESIAN_POINT ( 'NONE',  ( -30.58710530088973911, -25.14111132627482093, 7.291654623549845837 ) ) ;
#61968=CARTESIAN_POINT ( 'NONE',  ( 4.979423480801214552, 20.69870207611912605, -1.500000000000002220 ) ) ;
#61969=CARTESIAN_POINT ( 'NONE',  ( -31.24388727629348139, -25.01186361887644694, 7.715500679490839175 ) ) ;
#61970=LINE ( 'NONE', #14769, #40028 ) ;
#61971=CARTESIAN_POINT ( 'NONE',  ( -53.62287095715005592, -24.66019654487199375, 8.947790411086135265 ) ) ;
#61972=CARTESIAN_POINT ( 'NONE',  ( -71.31538854159695973, -25.28687673834294003, 5.910757521653128066 ) ) ;
#61973=CARTESIAN_POINT ( 'NONE',  ( 3.368619518803146029, -22.26131067175759881, -1.500000000000002220 ) ) ;
#61975=B_SPLINE_SURFACE_WITH_KNOTS ( 'NONE', 3, 1, ( 
 ( #93362, #23853 ),
 ( #16250, #85763 ),
 ( #79144, #40093 ),
 ( #8643, #32477 ),
 ( #39588, #24857 ),
 ( #70540, #3540 ),
 ( #96877, #63961 ),
 ( #88272, #58328 ),
 ( #41102, #2539 ),
 ( #27368, #79642 ),
 ( #34979, #94869 ),
 ( #10643, #65458 ),
 ( #50706, #41605 ),
 ( #10139, #73055 ),
 ( #87770, #89265 ) ),
 .UNSPECIFIED., .F., .F., .F.,
 ( 4, 1, 1, 1, 1, 1, 1, 1, 1, 1, 1, 1, 4 ),
 ( 2, 2 ),
 ( 0.000000000000000000, 0.1128134007444583364, 0.2253938839207267619, 0.3395948145626991321, 0.4596754102248635232, 0.5217351900879312332, 0.5839258387389140159, 0.6481741447653686095, 0.7138810381130654692, 0.7810044549073892339, 0.8514509275565547153, 0.9240506926641780527, 0.9999999999999998890 ),
 ( 0.000000000000000000, 1.000000000000000000 ),
 .UNSPECIFIED. ) ;
#61976=CARTESIAN_POINT ( 'NONE',  ( -110.9395002407040636, -25.32390614315827193, 4.358500768180118889 ) ) ;
#61978=CARTESIAN_POINT ( 'NONE',  ( -98.92287095715006728, -23.47593901973090524, -1.443836447538996648 ) ) ;
#61979=CARTESIAN_POINT ( 'NONE',  ( -9.247272915838292917, -17.29429475886123768, 11.49999999999999645 ) ) ;
#61980=CARTESIAN_POINT ( 'NONE',  ( -124.6228709571500559, -29.50250243563736774, 8.947779886222134493 ) ) ;
#61982=ORIENTED_EDGE ( 'NONE', *, *, #73259, .T. ) ;
#61983=CARTESIAN_POINT ( 'NONE',  ( -99.62727921284333377, -24.34968618360934300, 0.1864209137778966852 ) ) ;
#61985=CARTESIAN_POINT ( 'NONE',  ( -89.90192472445558280, -25.25787539255926717, 3.590294762828090125 ) ) ;
#61986=CARTESIAN_POINT ( 'NONE',  ( 3.912202881759007767, 19.34271161525698091, -1.500000000000002220 ) ) ;
#61990=ADVANCED_FACE ( 'NONE', ( #30371 ), #62338, .T. ) ;
#61993=PLANE ( 'NONE',  #9500 ) ;
#61994=CARTESIAN_POINT ( 'NONE',  ( -48.62287095715004881, -24.64965695001467694, 8.947790433994185832 ) ) ;
#62000=CARTESIAN_POINT ( 'NONE',  ( -7.473237707827510512, 18.53023608995856009, -1.500000000000002220 ) ) ;
#62001=CARTESIAN_POINT ( 'NONE',  ( -50.62287095715005592, -23.48786465467241058, 11.44779295918255180 ) ) ;
#62002=CARTESIAN_POINT ( 'NONE',  ( -45.48766593856211671, -24.52399227489127043, 9.353111116836528183 ) ) ;
#62006=DIRECTION ( 'NONE',  ( 0.000000000000000000, 0.9999999999976377785, 2.173523156925979128E-06 ) ) ;
#62007=CARTESIAN_POINT ( 'NONE',  ( -109.7130628311247591, -25.18430198549888388, 3.499763365511714408 ) ) ;
#62008=CARTESIAN_POINT ( 'NONE',  ( -35.56111601897774932, -23.85016227208580730, -0.8807180028928170978 ) ) ;
#62009=CARTESIAN_POINT ( 'NONE',  ( -28.62287095715004526, -24.50732993938405357, 8.947790418389013567 ) ) ;
#62011=CARTESIAN_POINT ( 'NONE',  ( -83.50069094083774246, -24.65952944569304606, 1.056160979905700126 ) ) ;
#62018=CARTESIAN_POINT ( 'NONE',  ( -12.21837793623082113, -16.16665877782589433, -1.500000000000002220 ) ) ;
#62019=VECTOR ( 'NONE', #93632, 1000.000000000000114 ) ;
#62020=B_SPLINE_CURVE_WITH_KNOTS ( 'NONE', 3,
 ( #42371, #89025, #2800, #33736 ),
 .UNSPECIFIED., .F., .F.,
 ( 4, 4 ),
 ( 0.000000000000000000, 0.0001000000000000167422 ),
 .UNSPECIFIED. ) ;
#62021=CARTESIAN_POINT ( 'NONE',  ( -28.62287095715006657, -24.50666107542846461, 1.056161637124864550 ) ) ;
#62023=CARTESIAN_POINT ( 'NONE',  ( -105.6228709571500275, -25.00158670708909625, 2.256160236439166411 ) ) ;
#62024=EDGE_CURVE ( 'NONE', #100004, #17029, #30875, .T. ) ;
#62027=CARTESIAN_POINT ( 'NONE',  ( -14.78635263257777233, 13.65558988533819473, -1.500000000000002220 ) ) ;
#62028=CARTESIAN_POINT ( 'NONE',  ( 2.841100885065937387, 20.89556961663114265, 11.49999999999999645 ) ) ;
#62030=CARTESIAN_POINT ( 'NONE',  ( 18.18892703665305177, -12.56521834855340281, 11.49999999999998934 ) ) ;
#62031=CARTESIAN_POINT ( 'NONE',  ( -20.49763986188970932, -1.003951800832726615, 11.49999999999998934 ) ) ;
#62034=FACE_OUTER_BOUND ( 'NONE', #83267, .T. ) ;
#62035=ORIENTED_EDGE ( 'NONE', *, *, #55861, .T. ) ;
#62036=CARTESIAN_POINT ( 'NONE',  ( -54.62287095715005592, -29.50250786944525672, 11.44777988621624054 ) ) ;
#62039=CARTESIAN_POINT ( 'NONE',  ( -85.62287095715008434, -24.63345952396257488, 9.038047939301511846 ) ) ;
#62040=ORIENTED_EDGE ( 'NONE', *, *, #65617, .F. ) ;
#62041=ORIENTED_EDGE ( 'NONE', *, *, #50882, .T. ) ;
#62042=ORIENTED_EDGE ( 'NONE', *, *, #50484, .F. ) ;
#62046=CARTESIAN_POINT ( 'NONE',  ( -20.60850594246137035, -0.7621957659720622891, -1.500000000000002220 ) ) ;
#62047=EDGE_CURVE ( 'NONE', #48068, #2401, #96915, .T. ) ;
#62048=CARTESIAN_POINT ( 'NONE',  ( 20.07693369621832602, 7.961103810760662647, 11.49999999999999645 ) ) ;
#62050=VECTOR ( 'NONE', #9760, 1000.000000000000114 ) ;
#62051=CARTESIAN_POINT ( 'NONE',  ( -88.52287095715006160, -24.64898659630367916, 1.056161002820827921 ) ) ;
#62053=CARTESIAN_POINT ( 'NONE',  ( -20.95026660567425481, -7.857139728745305973, 11.49999999999998934 ) ) ;
#62054=CARTESIAN_POINT ( 'NONE',  ( -47.63366713346987069, -24.35071581493542325, 9.817618358456030592 ) ) ;
#62057=CARTESIAN_POINT ( 'NONE',  ( -99.52764846858842418, -25.27419814425944011, 3.999772249604663710 ) ) ;
#62058=CARTESIAN_POINT ( 'NONE',  ( -49.66060423489871312, -23.48786465467241058, 11.44779295918254824 ) ) ;
#62059=VECTOR ( 'NONE', #53634, 1000.000000000000227 ) ;
#62060=DIRECTION ( 'NONE',  ( -3.773278334453079030E-23, 0.9999999999976377785, 2.173523156925979128E-06 ) ) ;
#62061=CARTESIAN_POINT ( 'NONE',  ( 10.02768300834196502, -18.34552750054021786, -1.500000000000002220 ) ) ;
#62062=ORIENTED_EDGE ( 'NONE', *, *, #31082, .T. ) ;
#62063=CARTESIAN_POINT ( 'NONE',  ( -45.52287095715006160, -24.99156044556202616, 7.747789690856173195 ) ) ;
#62064=EDGE_CURVE ( 'NONE', #92642, #41756, #60349, .T. ) ;
#62067=CARTESIAN_POINT ( 'NONE',  ( -10.94853654022341516, 18.13385389444049522, -1.500000000000002220 ) ) ;
#62070=CARTESIAN_POINT ( 'NONE',  ( -50.48973103951670538, -24.52300882791529801, 0.6510814631126389251 ) ) ;
#62071=B_SPLINE_CURVE_WITH_KNOTS ( 'NONE', 3,
 ( #89444, #74218, #19426, #59005, #65633, #96549 ),
 .UNSPECIFIED., .F., .F.,
 ( 4, 2, 4 ),
 ( 6.384118678610336992E-06, 0.001386860460828373684, 0.002767336802978137122 ),
 .UNSPECIFIED. ) ;
#62072=CARTESIAN_POINT ( 'NONE',  ( 4.771108217193557266, 21.26182814020628697, 11.49999999999998934 ) ) ;
#62074=CARTESIAN_POINT ( 'NONE',  ( -48.52287095715006160, -24.65952944569304606, 1.056160979905693686 ) ) ;
#62075=CARTESIAN_POINT ( 'NONE',  ( -79.34891651374461219, -25.27186867375041857, 6.035758440376426393 ) ) ;
#62076=CARTESIAN_POINT ( 'NONE',  ( -1.534710021792092594, -21.76038796025502009, -1.500000000000002220 ) ) ;
#62077=CARTESIAN_POINT ( 'NONE',  ( -30.57287095715007297, -24.98095046702749755, 2.202836320189033081 ) ) ;
#62078=ORIENTED_EDGE ( 'NONE', *, *, #67258, .F. ) ;
#62079=CARTESIAN_POINT ( 'NONE',  ( -30.51964735150444241, -23.47802267728122416, 11.44779284538084241 ) ) ;
#62080=CARTESIAN_POINT ( 'NONE',  ( -66.52287095715006160, -29.50248528299804818, 1.056150453629036701 ) ) ;
#62083=EDGE_CURVE ( 'NONE', #63420, #67116, #90801, .T. ) ;
#62084=EDGE_LOOP ( 'NONE', ( #92989, #2321, #39240, #41090 ) ) ;
#62089=DIRECTION ( 'NONE',  ( -3.773278334453079030E-23, 0.9999999999976377785, 2.173523156925979128E-06 ) ) ;
#62091=CARTESIAN_POINT ( 'NONE',  ( 7.993063233546146229, -19.64520799392144568, -1.500000000000002220 ) ) ;
#62092=CARTESIAN_POINT ( 'NONE',  ( -94.58633464317938433, -24.51314013834315375, 0.6176544820404151759 ) ) ;
#62093=CARTESIAN_POINT ( 'NONE',  ( -79.32136430576915131, -25.03138187970275652, 7.049788599829707181 ) ) ;
#62094=CARTESIAN_POINT ( 'NONE',  ( -59.62287095715004881, -24.66019654487199020, 8.947790411086131712 ) ) ;
#62096=AXIS2_PLACEMENT_3D ( 'NONE', #92151, #28268, #21632 ) ;
#62097=CARTESIAN_POINT ( 'NONE',  ( 19.02374887324148389, -3.781047496429098764, 11.49999999999998934 ) ) ;
#62098=EDGE_CURVE ( 'NONE', #89773, #79651, #59464, .T. ) ;
#62099=CARTESIAN_POINT ( 'NONE',  ( -69.75924279648913284, -25.30665621374858532, 5.475492409637942259 ) ) ;
#62100=ORIENTED_EDGE ( 'NONE', *, *, #40303, .F. ) ;
#62101=CARTESIAN_POINT ( 'NONE',  ( -12.17249226084429203, 15.20430173202493940, 11.49999999999999645 ) ) ;
#62102=LINE ( 'NONE', #22504, #21216 ) ;
#62104=VERTEX_POINT ( 'NONE', #422 ) ;
#62107=CARTESIAN_POINT ( 'NONE',  ( -91.62287095715004170, -24.64965695001468404, 8.947790433994180503 ) ) ;
#62108=CARTESIAN_POINT ( 'NONE',  ( -55.62287095715007013, -24.83602698348158810, 1.605859176311264847 ) ) ;
#62109=CARTESIAN_POINT ( 'NONE',  ( 13.10555085358618221, -14.64361678476065087, 11.49999999999998934 ) ) ;
#62110=B_SPLINE_SURFACE_WITH_KNOTS ( 'NONE', 3, 1, ( 
 ( #13022, #20144 ),
 ( #28763, #29253 ),
 ( #6916, #59726 ),
 ( #98760, #13522 ),
 ( #43500, #82542 ) ),
 .UNSPECIFIED., .F., .F., .F.,
 ( 4, 1, 4 ),
 ( 2, 2 ),
 ( 0.000000000000000000, 0.5078576360847800730, 1.000000000000000000 ),
 ( 0.000000000000000000, 1.000000000000000000 ),
 .UNSPECIFIED. ) ;
#62113=CARTESIAN_POINT ( 'NONE',  ( 20.63042821663210091, 6.393326493806346100, -1.500000000000002220 ) ) ;
#62114=CARTESIAN_POINT ( 'NONE',  ( -95.52287095715009002, -24.52323809116984421, 9.355190652339429036 ) ) ;
#62115=CARTESIAN_POINT ( 'NONE',  ( -40.64478534806120535, -24.40034930558990922, 0.3402023900116037392 ) ) ;
#62117=CARTESIAN_POINT ( 'NONE',  ( -17.14199295335891904, -15.44578658782692671, -1.500000000000002220 ) ) ;
#62119=CARTESIAN_POINT ( 'NONE',  ( -93.50973692245648294, -24.34968618360934656, 0.1864209137778838343 ) ) ;
#62121=CARTESIAN_POINT ( 'NONE',  ( -121.6275764894026423, -23.48786465467241413, 11.44779295918253581 ) ) ;
#62122=CARTESIAN_POINT ( 'NONE',  ( -64.62287095715005592, -24.66019654487198665, 8.947790411086131712 ) ) ;
#62123=CARTESIAN_POINT ( 'NONE',  ( -109.4873253428160922, -25.23964128780368554, 3.732949821448104721 ) ) ;
#62124=CARTESIAN_POINT ( 'NONE',  ( -129.5556841849855232, -24.65952944569305316, 1.056160979905705899 ) ) ;
#62125=CARTESIAN_POINT ( 'NONE',  ( -99.12529836037420239, -25.31565907717662967, 4.049155208725341737 ) ) ;
#62126=CARTESIAN_POINT ( 'NONE',  ( 19.57267778704439820, -3.578973306870405047, -1.500000000000002220 ) ) ;
#62128=CARTESIAN_POINT ( 'NONE',  ( -118.5562042904833930, -23.48786465467241769, 11.44779295918253403 ) ) ;
#62129=CARTESIAN_POINT ( 'NONE',  ( -2.735935421901279696, -19.66989661884619522, -1.500000000000002220 ) ) ;
#62131=CARTESIAN_POINT ( 'NONE',  ( -39.44256650533377950, -25.10925678386670157, 3.228028143694820606 ) ) ;
#62132=CARTESIAN_POINT ( 'NONE',  ( -35.62287095715006302, -23.84081130438200091, 10.88220057463248835 ) ) ;
#62133=CARTESIAN_POINT ( 'NONE',  ( 20.09396958936853395, 5.161349618257207617, 11.49999999999999645 ) ) ;
#62135=CARTESIAN_POINT ( 'NONE',  ( -78.52287095715004739, -23.95044443724992078, 10.65354141964648704 ) ) ;
#62136=CARTESIAN_POINT ( 'NONE',  ( 2.720868037236281012, -22.60253418658637869, 11.49999999999999645 ) ) ;
#62138=ADVANCED_FACE ( 'NONE', ( #68939 ), #22743, .F. ) ;
#62139=CARTESIAN_POINT ( 'NONE',  ( -57.62287095715003460, -24.65952944569304606, 1.056160979905696573 ) ) ;
#62140=CARTESIAN_POINT ( 'NONE',  ( -92.52287095715007581, -24.50321055353804667, 9.387540953477515160 ) ) ;
#62141=ADVANCED_FACE ( 'NONE', ( #71452 ), #10536, .F. ) ;
#62143=CARTESIAN_POINT ( 'NONE',  ( -19.13055903301823335, -6.388282315271819556, 11.49999999999998934 ) ) ;
#62144=LINE ( 'NONE', #85459, #54870 ) ;
#62146=CARTESIAN_POINT ( 'NONE',  ( -95.62287095715004170, -24.51163499207176244, 0.6490370598554217052 ) ) ;
#62147=ADVANCED_FACE ( 'NONE', ( #47613 ), #93770, .F. ) ;
#62150=EDGE_LOOP ( 'NONE', ( #45715, #70424, #89904, #71171 ) ) ;
#62152=CARTESIAN_POINT ( 'NONE',  ( -97.62287095715005592, -23.47593901973091235, -1.443836447539001089 ) ) ;
#62153=CARTESIAN_POINT ( 'NONE',  ( -2.380104427745746154, 22.76713797270899065, 11.49999999999998934 ) ) ;
#62154=CARTESIAN_POINT ( 'NONE',  ( -50.40445135320379677, -25.27420563080442406, 3.293942922663647632 ) ) ;
#62155=CARTESIAN_POINT ( 'NONE',  ( 5.966611984012316405, 20.80180421262142687, -1.500000000000002220 ) ) ;
#62156=DIRECTION ( 'NONE',  ( -3.773278334444167608E-23, 1.000000000000000000, 0.000000000000000000 ) ) ;
#62157=CARTESIAN_POINT ( 'NONE',  ( 0.8316226063609513108, 20.92010288561657205, 11.49999999999999645 ) ) ;
#62158=VERTEX_POINT ( 'NONE', #72450 ) ;
#62160=CARTESIAN_POINT ( 'NONE',  ( -124.6242032400218704, -24.34968618360933945, 0.1864209137778899961 ) ) ;
#62161=CARTESIAN_POINT ( 'NONE',  ( -21.99024891984110752, 1.279939690139831665, -1.500000000000002220 ) ) ;
#62163=CARTESIAN_POINT ( 'NONE',  ( -30.47287095715007865, -25.30734145635176802, 5.571384887382079043 ) ) ;
#62164=ORIENTED_EDGE ( 'NONE', *, *, #57927, .T. ) ;
#62166=CARTESIAN_POINT ( 'NONE',  ( -67.52287095715006160, -24.64898659630528854, 1.056161002820824368 ) ) ;
#62169=ORIENTED_EDGE ( 'NONE', *, *, #280, .F. ) ;
#62172=CARTESIAN_POINT ( 'NONE',  ( -71.55916567469419931, -23.73791477778911840, 11.05961554403170766 ) ) ;
#62173=CARTESIAN_POINT ( 'NONE',  ( -101.5300974081266787, -25.10935923999858588, 3.391563287084827127 ) ) ;
#62175=CARTESIAN_POINT ( 'NONE',  ( 18.81987132735423174, -8.002443037797982939, -1.500000000000002220 ) ) ;
#62178=CARTESIAN_POINT ( 'NONE',  ( -61.58953762381671737, -23.47596703998600276, 11.44779298504227505 ) ) ;
#62179=CARTESIAN_POINT ( 'NONE',  ( -100.5228709571500616, -24.99132157543084531, 2.256160258750667502 ) ) ;
#62181=CARTESIAN_POINT ( 'NONE',  ( 20.80681148587913754, 8.022540738981085440, -1.500000000000002220 ) ) ;
#62183=CARTESIAN_POINT ( 'NONE',  ( -26.80445111962029614, -24.62944456348768796, 8.034172700478890761 ) ) ;
#62184=EDGE_CURVE ( 'NONE', #55923, #75111, #27901, .T. ) ;
#62185=VERTEX_POINT ( 'NONE', #66228 ) ;
#62187=CARTESIAN_POINT ( 'NONE',  ( -29.77636857527935277, -25.26247541502187488, 5.788902928198627507 ) ) ;
#62188=CARTESIAN_POINT ( 'NONE',  ( 3.748101851616784774, 20.49759516964078188, 11.49999999999998934 ) ) ;
#62189=ORIENTED_EDGE ( 'NONE', *, *, #92398, .F. ) ;
#62192=ORIENTED_EDGE ( 'NONE', *, *, #48393, .T. ) ;
#62193=B_SPLINE_SURFACE_WITH_KNOTS ( 'NONE', 3, 3, ( 
 ( #18053, #11939, #3845, #80455 ),
 ( #34785, #65756, #72353, #10947 ),
 ( #2849, #26166, #49523, #41912 ),
 ( #96674, #27174, #58135, #34290 ),
 ( #58623, #73841, #4341, #35291 ),
 ( #66256, #89568, #76315, #13925 ),
 ( #44399, #67242, #91056, #91552 ) ),
 .UNSPECIFIED., .F., .F., .F.,
 ( 4, 3, 4 ),
 ( 4, 4 ),
 ( 0.0004766839783818044361, 0.1029713700210893312, 0.2054660560637968647 ),
 ( 0.8096999710875462108, 0.8110862897224703216 ),
 .UNSPECIFIED. ) ;
#62194=CARTESIAN_POINT ( 'NONE',  ( -119.5228709571500758, -23.47596703998600631, 11.44779298504227860 ) ) ;
#62195=CARTESIAN_POINT ( 'NONE',  ( 20.92198360912786015, -1.804805560479522342, -1.500000000000002220 ) ) ;
#62196=ORIENTED_EDGE ( 'NONE', *, *, #19902, .F. ) ;
#62198=CARTESIAN_POINT ( 'NONE',  ( -55.62287095715004170, -24.99156045073392463, 7.747789690856161648 ) ) ;
#62200=DIRECTION ( 'NONE',  ( -3.773278334453079618E-23, 0.9999999999976377785, 2.173523156925979975E-06 ) ) ;
#62201=CARTESIAN_POINT ( 'NONE',  ( -92.58613717802586507, -24.51419770103156281, 9.386484678747175181 ) ) ;
#62203=CARTESIAN_POINT ( 'NONE',  ( 19.10802705166043580, 11.29804532628753044, 11.49999999999999645 ) ) ;
#62209=CARTESIAN_POINT ( 'NONE',  ( 8.854694546379761277, 20.84150027139232364, -1.500000000000002220 ) ) ;
#62211=CARTESIAN_POINT ( 'NONE',  ( -115.5200931463694332, -23.85049219812686871, 10.88485053497526778 ) ) ;
#62216=EDGE_CURVE ( 'NONE', #46658, #76257, #85942, .T. ) ;
#62217=CARTESIAN_POINT ( 'NONE',  ( 17.11712468798820908, 10.61635618877791742, 11.49999999999998934 ) ) ;
#62218=CARTESIAN_POINT ( 'NONE',  ( -81.62287095715004170, -23.96177878511307568, 10.65340807706330217 ) ) ;
#62221=CARTESIAN_POINT ( 'NONE',  ( -13.97600220251353953, -17.46790257487896270, -1.500000000000002220 ) ) ;
#62222=EDGE_CURVE ( 'NONE', #15342, #1176, #95656, .T. ) ;
#62224=ORIENTED_EDGE ( 'NONE', *, *, #35685, .F. ) ;
#62225=CARTESIAN_POINT ( 'NONE',  ( -28.52287095715005805, -24.49960542107631056, 8.947790409070465856 ) ) ;
#62226=CARTESIAN_POINT ( 'NONE',  ( -94.58632622716793037, -24.51419770103156281, 9.386484678747184063 ) ) ;
#62227=CARTESIAN_POINT ( 'NONE',  ( -46.62287095715004881, -24.64965695001467694, 8.947790433994185832 ) ) ;
#62228=CARTESIAN_POINT ( 'NONE',  ( -57.55620429048337883, -24.64965694238574301, 8.947790433994201820 ) ) ;
#62229=B_SPLINE_CURVE_WITH_KNOTS ( 'NONE', 3,
 ( #3113, #64024, #25927, #28298 ),
 .UNSPECIFIED., .F., .F.,
 ( 4, 4 ),
 ( 0.000000000000000000, 9.999999999999593903E-05 ),
 .UNSPECIFIED. ) ;
#62230=CARTESIAN_POINT ( 'NONE',  ( -100.5228709571500616, -29.50249982740957577, 7.747779886224967605 ) ) ;
#62231=CARTESIAN_POINT ( 'NONE',  ( -8.292788067677484776, 17.68049324621676632, 11.49999999999998934 ) ) ;
#62232=CARTESIAN_POINT ( 'NONE',  ( -38.92287095715006728, -23.47596703998600276, 11.44779298504227683 ) ) ;
#62233=CARTESIAN_POINT ( 'NONE',  ( 20.96596170256846747, -4.772324250704091497, -1.500000000000002220 ) ) ;
#62234=CARTESIAN_POINT ( 'NONE',  ( -128.6237110843704841, -24.34968618360935011, 0.1864209137779018477 ) ) ;
#62238=CARTESIAN_POINT ( 'NONE',  ( -1.055347110731411187, -22.84297022578905612, -1.500000000000002220 ) ) ;
#62240=CARTESIAN_POINT ( 'NONE',  ( -96.51886295441239838, -23.73791477778912196, 11.05961554403170410 ) ) ;
#62242=CARTESIAN_POINT ( 'NONE',  ( -12.65591448191638335, 15.52279176289047236, 11.49999999999999645 ) ) ;
#62243=CARTESIAN_POINT ( 'NONE',  ( -116.6228709571500559, -29.50248528299804818, 1.056150453629045360 ) ) ;
#62246=DIRECTION ( 'NONE',  ( -3.773278334453079618E-23, 0.9999999999976377785, 2.173523156925979975E-06 ) ) ;
#62247=ORIENTED_EDGE ( 'NONE', *, *, #76885, .T. ) ;
#62248=CARTESIAN_POINT ( 'NONE',  ( -109.5228709571500616, -23.47596703998600631, 11.44779298504228038 ) ) ;
#62249=CARTESIAN_POINT ( 'NONE',  ( -108.9572686384559717, -25.27089656451258293, 4.080339631227976049 ) ) ;
#62250=CARTESIAN_POINT ( 'NONE',  ( 17.47290450027814757, -12.96279059203284767, -1.500000000000002220 ) ) ;
#62251=CARTESIAN_POINT ( 'NONE',  ( -56.62287095715007723, -23.96177878511307568, 10.65340807706329862 ) ) ;
#62252=CARTESIAN_POINT ( 'NONE',  ( 16.02095076306289201, 11.36058263404076030, -1.500000000000002220 ) ) ;
#62253=CARTESIAN_POINT ( 'NONE',  ( -128.6228709571500417, -24.64898659630529565, 1.056161002820834804 ) ) ;
#62254=CARTESIAN_POINT ( 'NONE',  ( -109.3584176993576591, -25.31697944907574538, 4.206202445080533536 ) ) ;
#62256=CARTESIAN_POINT ( 'NONE',  ( -56.62287095715005592, -23.72773821059536559, 11.05748984161097503 ) ) ;
#62258=CARTESIAN_POINT ( 'NONE',  ( 9.245221688665949955, -18.36014492602614467, 11.49999999999999645 ) ) ;
#62259=DIRECTION ( 'NONE',  ( -3.773278334453079030E-23, 0.9999999999976377785, 2.173523156925979128E-06 ) ) ;
#62261=CARTESIAN_POINT ( 'NONE',  ( -47.62287095715008434, -23.96127896941632685, -0.6493128931037891460 ) ) ;
#62262=EDGE_LOOP ( 'NONE', ( #75354, #53414, #27830, #38328 ) ) ;
#62263=EDGE_CURVE ( 'NONE', #33073, #16993, #54495, .T. ) ;
#62264=CARTESIAN_POINT ( 'NONE',  ( -80.80810426221744081, -25.29535151472738264, 4.196860092590704028 ) ) ;
#62265=CARTESIAN_POINT ( 'NONE',  ( -40.06853693287165186, -25.18430885312715617, 3.358278162901255026 ) ) ;
#62266=CARTESIAN_POINT ( 'NONE',  ( -97.56097956155602446, -23.48783264082477729, -1.443836473390088138 ) ) ;
#62269=CARTESIAN_POINT ( 'NONE',  ( -26.05468383228075169, -24.93063430545317516, 7.311465254594289753 ) ) ;
#62270=EDGE_CURVE ( 'NONE', #95575, #81379, #29155, .T. ) ;
#62273=ORIENTED_EDGE ( 'NONE', *, *, #73195, .F. ) ;
#62274=CARTESIAN_POINT ( 'NONE',  ( 21.06059016766346659, 9.494407541345388779, 11.49999999999999645 ) ) ;
#62275=CARTESIAN_POINT ( 'NONE',  ( 21.74077840044056842, -6.890983112422549794, 11.49999999999998934 ) ) ;
#62276=CARTESIAN_POINT ( 'NONE',  ( -74.63035518566482551, -24.34968618360933945, 0.1864209137778816139 ) ) ;
#62278=CARTESIAN_POINT ( 'NONE',  ( -96.56113055612571827, -23.48783264082477018, -1.443836473390089914 ) ) ;
#62279=CARTESIAN_POINT ( 'NONE',  ( -61.24303308397303880, -25.03284409833926105, 7.563174216509380265 ) ) ;
#62280=CARTESIAN_POINT ( 'NONE',  ( -8.519796113377745783, 20.75715399588506926, 11.49999999999999645 ) ) ;
#62281=VERTEX_POINT ( 'NONE', #74797 ) ;
#62282=CARTESIAN_POINT ( 'NONE',  ( -69.58953762381672448, -24.65952944569304606, 1.056160979905704567 ) ) ;
#62284=CARTESIAN_POINT ( 'NONE',  ( 0.1985894851802381678, 21.93841921393417849, -1.500000000000002220 ) ) ;
#62285=B_SPLINE_CURVE_WITH_KNOTS ( 'NONE', 3,
 ( #95759, #1423, #79024, #24243, #49105, #78013, #78516, #33863, #17636, #71433, #79533, #32358, #9023, #31866, #1922, #48608, #9522, #40980, #86645, #71940, #25243, #87147 ),
 .UNSPECIFIED., .F., .F.,
 ( 4, 2, 2, 2, 2, 2, 2, 2, 2, 2, 4 ),
 ( 0.000000000000000000, 0.0002789520332696046362, 0.0005579040665392092724, 0.0008368560998088139628, 0.001115808133078418545, 0.001673712199617617300, 0.002231616266156815839, 0.002789520332696014595, 0.003347424399235213784, 0.003905328465774412540, 0.004463232532313610862 ),
 .UNSPECIFIED. ) ;
#62287=CARTESIAN_POINT ( 'NONE',  ( -44.58159999861633338, -24.51419770103159834, 9.386484678747169852 ) ) ;
#62289=ORIENTED_EDGE ( 'NONE', *, *, #99229, .F. ) ;
#62292=EDGE_LOOP ( 'NONE', ( #100350, #17232, #16465, #72280 ) ) ;
#62293=CARTESIAN_POINT ( 'NONE',  ( 1.259202695315177589, 20.44674571593545664, 11.49999999999998934 ) ) ;
#62294=EDGE_LOOP ( 'NONE', ( #58795, #33500, #99123, #54813 ) ) ;
#62295=ORIENTED_EDGE ( 'NONE', *, *, #43217, .T. ) ;
#62296=ORIENTED_EDGE ( 'NONE', *, *, #16133, .T. ) ;
#62297=VERTEX_POINT ( 'NONE', #91027 ) ;
#62298=CARTESIAN_POINT ( 'NONE',  ( -13.34915495237762251, 18.83725853537101358, 11.49999999999998934 ) ) ;
#62299=CARTESIAN_POINT ( 'NONE',  ( -49.17688710052657797, -25.23571112353340595, 3.608735733131122281 ) ) ;
#62300=CARTESIAN_POINT ( 'NONE',  ( 18.81862293822770837, 7.596102252255398035, -1.500000000000002220 ) ) ;
#62302=FACE_OUTER_BOUND ( 'NONE', #30728, .T. ) ;
#62303=CARTESIAN_POINT ( 'NONE',  ( -92.58398966098822314, -24.65952944569303895, 1.056160979905702346 ) ) ;
#62304=DIRECTION ( 'NONE',  ( 0.000000000000000000, -2.173523156925980399E-06, 0.9999999999976378895 ) ) ;
#62306=CARTESIAN_POINT ( 'NONE',  ( -5.860608850286626925, 20.67097946995454905, 11.49999999999999645 ) ) ;
#62308=CARTESIAN_POINT ( 'NONE',  ( -75.49536848232909847, -24.73486907724918282, 1.287355809206967683 ) ) ;
#62309=CARTESIAN_POINT ( 'NONE',  ( -61.58759230001847129, -24.35071581493543036, 9.817618358456030592 ) ) ;
#62311=ORIENTED_EDGE ( 'NONE', *, *, #88871, .F. ) ;
#62312=CARTESIAN_POINT ( 'NONE',  ( 20.56943099487245519, -2.726235779781958968, -1.500000000000002220 ) ) ;
#62315=ORIENTED_EDGE ( 'NONE', *, *, #18839, .T. ) ;
#62316=CARTESIAN_POINT ( 'NONE',  ( -111.5905771631722843, -24.15620529776629510, 10.23563542870659582 ) ) ;
#62317=B_SPLINE_CURVE_WITH_KNOTS ( 'NONE', 3,
 ( #44358, #35743, #19504, #73307 ),
 .UNSPECIFIED., .F., .F.,
 ( 4, 4 ),
 ( 0.000000000000000000, 1.000000000000000000 ),
 .UNSPECIFIED. ) ;
#62320=EDGE_LOOP ( 'NONE', ( #74846, #5473, #7799, #3396 ) ) ;
#62321=CARTESIAN_POINT ( 'NONE',  ( -55.52287095715005449, -24.99156044556119483, 7.747789690856173195 ) ) ;
#62322=CARTESIAN_POINT ( 'NONE',  ( -77.62287095715007013, -23.95044443724992433, 10.65354141964650125 ) ) ;
#62324=CARTESIAN_POINT ( 'NONE',  ( -21.92701646642465008, -2.088449908657787457, 11.49999999999999645 ) ) ;
#62325=DIRECTION ( 'NONE',  ( -3.773278334453079030E-23, 0.9999999999976377785, 2.173523156925979128E-06 ) ) ;
#62326=CARTESIAN_POINT ( 'NONE',  ( -1.585881643086899606, 22.48459252949185228, -1.500000000000002220 ) ) ;
#62327=CARTESIAN_POINT ( 'NONE',  ( -2.639205680565387624, -20.84613592336672028, -1.500000000000002220 ) ) ;
#62328=LINE ( 'NONE', #69429, #57293 ) ;
#62329=VERTEX_POINT ( 'NONE', #12401 ) ;
#62330=EDGE_LOOP ( 'NONE', ( #81515, #83239, #52590, #52831 ) ) ;
#62332=EDGE_CURVE ( 'NONE', #75868, #19742, #21766, .T. ) ;
#62335=CARTESIAN_POINT ( 'NONE',  ( -113.6228709571501270, -23.95044443724993499, 10.65354141964649415 ) ) ;
#62337=CARTESIAN_POINT ( 'NONE',  ( 1.812468502196824760, -21.08352789287561180, 11.49999999999998934 ) ) ;
#62338=PLANE ( 'NONE',  #33568 ) ;
#62339=CARTESIAN_POINT ( 'NONE',  ( -51.06671402896819956, -25.03148719215326778, 7.458180231579937036 ) ) ;
#62340=CARTESIAN_POINT ( 'NONE',  ( -121.6245723567604813, -24.34968618360934300, 0.1864209137778885528 ) ) ;
#62341=CARTESIAN_POINT ( 'NONE',  ( -52.52287095715005449, -23.47593901973090524, -1.443836447538997092 ) ) ;
#62342=CARTESIAN_POINT ( 'NONE',  ( -127.5228709571500900, -24.51387760970726504, 9.387446482453405849 ) ) ;
#62343=CARTESIAN_POINT ( 'NONE',  ( -21.14055147415990277, -6.693858341896442354, -1.500000000000002220 ) ) ;
#62348=DIRECTION ( 'NONE',  ( -3.773278334453079030E-23, 0.9999999999976377785, 2.173523156925979128E-06 ) ) ;
#62349=CARTESIAN_POINT ( 'NONE',  ( -126.5206434123637393, -24.51314013834316086, 0.6176544820404181735 ) ) ;
#62351=DIRECTION ( 'NONE',  ( -3.773278334444167608E-23, 1.000000000000000000, 0.000000000000000000 ) ) ;
#62352=CARTESIAN_POINT ( 'NONE',  ( 14.64286990871793392, 12.78475832571431070, 11.49999999999998934 ) ) ;
#62353=CARTESIAN_POINT ( 'NONE',  ( 16.75108703964928480, -13.32659110743468212, 11.49999999999998934 ) ) ;
#62356=DIRECTION ( 'NONE',  ( -3.773278334444166432E-23, 1.000000000000000000, 0.000000000000000000 ) ) ;
#62357=CARTESIAN_POINT ( 'NONE',  ( -101.2905359165590227, -25.27360087335221550, 3.812648439097560793 ) ) ;
#62358=CARTESIAN_POINT ( 'NONE',  ( -21.72567761722203628, 6.514095075961352954, -1.500000000000002220 ) ) ;
#62359=CARTESIAN_POINT ( 'NONE',  ( -103.6228709571500701, -23.96127896941633750, -0.6493128931037811524 ) ) ;
#62360=CARTESIAN_POINT ( 'NONE',  ( -80.52287095715006160, -23.47593901973090169, -1.443836447538996648 ) ) ;
#62361=CARTESIAN_POINT ( 'NONE',  ( 17.59243620335545799, -9.192777620008959261, 11.49999999999999645 ) ) ;
#62362=CARTESIAN_POINT ( 'NONE',  ( -123.5900400688965561, -24.15620529776629866, 10.23563542870659582 ) ) ;
#62363=CARTESIAN_POINT ( 'NONE',  ( -88.52287095715006160, -24.64898659630367916, 1.056161002820827921 ) ) ;
#62364=VERTEX_POINT ( 'NONE', #76289 ) ;
#62365=FACE_OUTER_BOUND ( 'NONE', #41349, .T. ) ;
#62366=LINE ( 'NONE', #63385, #10215 ) ;
#62367=PLANE ( 'NONE',  #88507 ) ;
#62368=CARTESIAN_POINT ( 'NONE',  ( 11.52859134480388903, -18.33581920571378632, -1.500000000000002220 ) ) ;
#62370=CARTESIAN_POINT ( 'NONE',  ( -5.694372300836820777, 18.57635362771370424, -1.500000000000002220 ) ) ;
#62371=CARTESIAN_POINT ( 'NONE',  ( -55.58579905264048904, -24.63419186844611275, 9.035850630976927533 ) ) ;
#62372=EDGE_CURVE ( 'NONE', #24081, #99074, #91523, .T. ) ;
#62373=EDGE_LOOP ( 'NONE', ( #97526, #78509, #4045, #23616 ) ) ;
#62375=CARTESIAN_POINT ( 'NONE',  ( 14.85214116200856083, 13.97194181870810326, 11.49999999999999645 ) ) ;
#62376=CARTESIAN_POINT ( 'NONE',  ( -80.50908809528748122, -24.15503026093913164, -0.2815557561904567518 ) ) ;
#62377=B_SPLINE_CURVE_WITH_KNOTS ( 'NONE', 3,
 ( #28123, #43850, #4785, #57589, #67197, #98112 ),
 .UNSPECIFIED., .F., .F.,
 ( 4, 2, 4 ),
 ( 0.000000000000000000, 0.001380901958385390062, 0.002761803916770780125 ),
 .UNSPECIFIED. ) ;
#62380=CARTESIAN_POINT ( 'NONE',  ( -41.32712894388434677, -25.24779038991585267, 3.715000390373129679 ) ) ;
#62381=CARTESIAN_POINT ( 'NONE',  ( -92.52287095715010423, -24.33832256527049509, 0.1851278514138617326 ) ) ;
#62382=CARTESIAN_POINT ( 'NONE',  ( -49.27237840819080361, -25.31601884727480822, 5.251752407945899925 ) ) ;
#62384=DIRECTION ( 'NONE',  ( -3.773278334453079030E-23, 0.9999999999976377785, 2.173523156925979128E-06 ) ) ;
#62386=CARTESIAN_POINT ( 'NONE',  ( 12.55954966114946458, -15.69740789531843461, -1.500000000000002220 ) ) ;
#62390=CARTESIAN_POINT ( 'NONE',  ( -81.62287095715005592, -23.47593901973091235, -1.443836447539004642 ) ) ;
#62391=ADVANCED_FACE ( 'NONE', ( #75793 ), #22495, .F. ) ;
#62392=CARTESIAN_POINT ( 'NONE',  ( -9.520747347383798243, -20.79447232172871907, 11.49999999999999645 ) ) ;
#62393=CARTESIAN_POINT ( 'NONE',  ( -22.07869367785253090, -5.390224856484156390, 11.49999999999998934 ) ) ;
#62394=EDGE_LOOP ( 'NONE', ( #92298, #18713, #70978, #61697 ) ) ;
#62395=CARTESIAN_POINT ( 'NONE',  ( -30.47287095715007155, -24.75375236407085566, 8.603495955171387877 ) ) ;
#62398=CARTESIAN_POINT ( 'NONE',  ( -38.51305747304791538, -23.73791477778911485, 11.05961554403170766 ) ) ;
#62400=CARTESIAN_POINT ( 'NONE',  ( -30.57287095715007297, -25.31506640534328056, 5.571610402288234454 ) ) ;
#62402=B_SPLINE_CURVE_WITH_KNOTS ( 'NONE', 3,
 ( #59435, #5140, #27982, #74156 ),
 .UNSPECIFIED., .F., .F.,
 ( 4, 4 ),
 ( 0.000000000000000000, 9.999999999998897304E-05 ),
 .UNSPECIFIED. ) ;
#62404=CARTESIAN_POINT ( 'NONE',  ( -124.5228709571500900, -23.48783264082477373, -1.443836473390085029 ) ) ;
#62405=ORIENTED_EDGE ( 'NONE', *, *, #71872, .F. ) ;
#62406=CARTESIAN_POINT ( 'NONE',  ( 15.56926775127050000, -13.18612581554039132, -1.500000000000002220 ) ) ;
#62407=VERTEX_POINT ( 'NONE', #37740 ) ;
#62408=EDGE_CURVE ( 'NONE', #44155, #9237, #98630, .T. ) ;
#62409=B_SPLINE_CURVE_WITH_KNOTS ( 'NONE', 3,
 ( #42075, #50673, #34450, #10606, #12598, #35940, #97830, #81619, #28325, #80116, #59279, #90228 ),
 .UNSPECIFIED., .F., .F.,
 ( 4, 2, 2, 2, 2, 4 ),
 ( 4.336808689942017736E-18, 0.0001760285354383833852, 0.0003520570708767624337, 0.0007041141417535211810, 0.001056171212630279983, 0.001408228283507038676 ),
 .UNSPECIFIED. ) ;
#62410=CARTESIAN_POINT ( 'NONE',  ( -21.12268324108725892, 9.058254180033936009, -1.500000000000002220 ) ) ;
#62411=CARTESIAN_POINT ( 'NONE',  ( -54.56747899101539190, -23.48786465467240703, 11.44779295918255180 ) ) ;
#62416=B_SPLINE_CURVE_WITH_KNOTS ( 'NONE', 3,
 ( #25442, #49302, #18334, #72136, #2622, #33561, #95453, #10727, #41689, #3127, #65042, #78546, #40002, #25271 ),
 .UNSPECIFIED., .F., .F.,
 ( 4, 2, 2, 2, 2, 2, 4 ),
 ( 0.000000000000000000, 0.0002387142825911133296, 0.0004774285651822266592, 0.0009548571303644522341, 0.001432285695546677701, 0.001670999978137770701, 0.001909714260728863702 ),
 .UNSPECIFIED. ) ;
#62419=CARTESIAN_POINT ( 'NONE',  ( 17.02398533174402218, 12.79255474601471043, 11.49999999999999645 ) ) ;
#62421=ORIENTED_EDGE ( 'NONE', *, *, #76050, .T. ) ;
#62422=CARTESIAN_POINT ( 'NONE',  ( 16.02632597834478645, 15.35701383120132313, 11.49999999999998934 ) ) ;
#62423=CARTESIAN_POINT ( 'NONE',  ( 1.453578435135240321, -20.60874541997745268, 11.49999999999998934 ) ) ;
#62424=ORIENTED_EDGE ( 'NONE', *, *, #95705, .T. ) ;
#62425=ORIENTED_EDGE ( 'NONE', *, *, #82022, .F. ) ;
#62427=CARTESIAN_POINT ( 'NONE',  ( -71.72343159422317171, -25.32724624944561853, 4.398071659717722959 ) ) ;
#62428=ORIENTED_EDGE ( 'NONE', *, *, #79796, .F. ) ;
#62429=CARTESIAN_POINT ( 'NONE',  ( -91.58383859757618950, -24.65952944569304606, 1.056160979905701680 ) ) ;
#62430=EDGE_LOOP ( 'NONE', ( #90234, #39683, #83031, #13264 ) ) ;
#62431=CARTESIAN_POINT ( 'NONE',  ( -58.53810489024537844, -24.51419770103156637, 9.386484678747176957 ) ) ;
#62433=CARTESIAN_POINT ( 'NONE',  ( -3.686900873480770002, -20.48319827837541141, -1.500000000000002220 ) ) ;
#62434=CARTESIAN_POINT ( 'NONE',  ( 3.267597511969735802, 21.59432767039258394, 11.49999999999999645 ) ) ;
#62435=CARTESIAN_POINT ( 'NONE',  ( -91.94687923781920347, -25.22391124735684187, 6.409327647371628522 ) ) ;
#62436=CARTESIAN_POINT ( 'NONE',  ( -78.58481383403142218, -24.51419770103157347, 9.386484678747175181 ) ) ;
#62437=CARTESIAN_POINT ( 'NONE',  ( 12.99221220249228281, -18.32192329980629708, -1.500000000000002220 ) ) ;
#62438=CARTESIAN_POINT ( 'NONE',  ( -38.52201953751992392, -23.48783264082477729, -1.443836473390076591 ) ) ;
#62440=PLANE ( 'NONE',  #63110 ) ;
#62443=ORIENTED_EDGE ( 'NONE', *, *, #19983, .T. ) ;
#62444=ORIENTED_EDGE ( 'NONE', *, *, #61490, .T. ) ;
#62446=ORIENTED_EDGE ( 'NONE', *, *, #35715, .T. ) ;
#62447=CARTESIAN_POINT ( 'NONE',  ( -18.12654925440673637, -11.31956730046968751, -1.500000000000002220 ) ) ;
#62448=VERTEX_POINT ( 'NONE', #60104 ) ;
#62449=CARTESIAN_POINT ( 'NONE',  ( 21.00884048613226440, 1.293913838035418040, -1.500000000000002220 ) ) ;
#62450=CARTESIAN_POINT ( 'NONE',  ( -30.43338820629497476, -24.47561425214244224, 0.5642940035406436294 ) ) ;
#62451=B_SPLINE_CURVE_WITH_KNOTS ( 'NONE', 3,
 ( #82056, #13027, #5426, #36877 ),
 .UNSPECIFIED., .F., .F.,
 ( 4, 4 ),
 ( 0.5609005253356335041, 0.5699069566077490379 ),
 .UNSPECIFIED. ) ;
#62452=CARTESIAN_POINT ( 'NONE',  ( 11.38277053702107899, 16.36964821499295653, -1.500000000000002220 ) ) ;
#62453=CARTESIAN_POINT ( 'NONE',  ( -50.63202991560478949, -24.73531770709094602, 8.716586749053508498 ) ) ;
#62455=CARTESIAN_POINT ( 'NONE',  ( 12.33731239738771102, -18.22686410513083288, -1.500000000000002220 ) ) ;
#62456=CARTESIAN_POINT ( 'NONE',  ( -87.52287095715003318, -24.33832256527048088, 0.1851278514138628983 ) ) ;
#62457=EDGE_LOOP ( 'NONE', ( #1274, #70587, #97104, #24078 ) ) ;
#62458=DIRECTION ( 'NONE',  ( -3.773278334453079618E-23, 0.9999999999976377785, 2.173523156925979975E-06 ) ) ;
#62460=CARTESIAN_POINT ( 'NONE',  ( -12.81329989551134751, 16.42372500408851366, 11.49999999999999645 ) ) ;
#62462=CARTESIAN_POINT ( 'NONE',  ( -125.5228709571500616, -23.47596703998600631, 11.44779298504227683 ) ) ;
#62463=CARTESIAN_POINT ( 'NONE',  ( -56.55620429048338593, -23.48783264082477729, -1.443836473390068376 ) ) ;
#62464=CARTESIAN_POINT ( 'NONE',  ( -17.77299844720193533, 11.79293508692305537, 11.49999999999998934 ) ) ;
#62465=CARTESIAN_POINT ( 'NONE',  ( -31.24388727629348494, -25.12217695392594763, 7.176903142167552652 ) ) ;
#62466=CARTESIAN_POINT ( 'NONE',  ( -27.47983700607433732, -24.75185972549630264, 2.285866012509995215 ) ) ;
#62467=AXIS2_PLACEMENT_3D ( 'NONE', #12706, #43672, #67516 ) ;
#62471=CARTESIAN_POINT ( 'NONE',  ( -8.307687032909205627, 20.95097986170506488, -1.500000000000002220 ) ) ;
#62473=CARTESIAN_POINT ( 'NONE',  ( -110.9400161722045794, -25.25626643526282322, 3.571638612575482874 ) ) ;
#62475=CARTESIAN_POINT ( 'NONE',  ( -79.06619145297914031, -25.30163491681836874, 5.325055240909210674 ) ) ;
#62477=CARTESIAN_POINT ( 'NONE',  ( 15.15379598424239838, -12.58889634127381640, 11.49999999999999645 ) ) ;
#62479=VECTOR ( 'NONE', #95911, 1000.000000000000114 ) ;
#62480=CARTESIAN_POINT ( 'NONE',  ( -39.55620429048339304, -24.64898659630528499, 1.056161002820822370 ) ) ;
#62481=EDGE_LOOP ( 'NONE', ( #57202, #48565, #22281, #10872 ) ) ;
#62483=CARTESIAN_POINT ( 'NONE',  ( -99.59111762178828542, -24.15543982623907837, -0.2315651400026449425 ) ) ;
#62484=CARTESIAN_POINT ( 'NONE',  ( -42.55620429048339304, -24.64965694238574656, 8.947790433994203596 ) ) ;
#62485=CARTESIAN_POINT ( 'NONE',  ( -91.96772508908847499, -25.06732983082694233, 7.447789526168957508 ) ) ;
#62488=CARTESIAN_POINT ( 'NONE',  ( 5.037983044326730386, -19.10262670698400100, -1.500000000000002220 ) ) ;
#62489=VERTEX_POINT ( 'NONE', #22991 ) ;
#62490=CARTESIAN_POINT ( 'NONE',  ( -120.5228709571500900, -24.83620972994592435, 8.398175272781360334 ) ) ;
#62494=CARTESIAN_POINT ( 'NONE',  ( -53.62287095715006302, -23.72747288104441665, -1.053458166803663998 ) ) ;
#62496=CARTESIAN_POINT ( 'NONE',  ( -98.94109201664207376, -25.26638307310151532, 6.485444322923475724 ) ) ;
#62498=CARTESIAN_POINT ( 'NONE',  ( -36.62287095715005592, -29.50247984919015209, -1.443849546365060466 ) ) ;
#62500=CARTESIAN_POINT ( 'NONE',  ( -15.86121933104946535, 12.22609501325904624, -1.500000000000002220 ) ) ;
#62501=EDGE_CURVE ( 'NONE', #58389, #922, #73915, .T. ) ;
#62502=CARTESIAN_POINT ( 'NONE',  ( -99.12594121859551421, -25.27533104972792799, 3.952132688946379702 ) ) ;
#62503=CARTESIAN_POINT ( 'NONE',  ( -51.70072539166535108, -25.27314792116673203, 3.987152059579775809 ) ) ;
#62504=VERTEX_POINT ( 'NONE', #30620 ) ;
#62505=B_SPLINE_CURVE_WITH_KNOTS ( 'NONE', 3,
 ( #81000, #51057, #65308, #56685 ),
 .UNSPECIFIED., .F., .F.,
 ( 4, 4 ),
 ( 0.000000000000000000, 0.0001000000000000028644 ),
 .UNSPECIFIED. ) ;
#62508=CARTESIAN_POINT ( 'NONE',  ( -110.2348554541972874, -25.29012726010009970, 3.296590529549364490 ) ) ;
#62510=PLANE ( 'NONE',  #57491 ) ;
#62512=EDGE_CURVE ( 'NONE', #48580, #74478, #145, .T. ) ;
#62513=CARTESIAN_POINT ( 'NONE',  ( -34.52287095715006160, -29.50250243563736774, 8.947779886222150481 ) ) ;
#62514=CARTESIAN_POINT ( 'NONE',  ( -83.50635389765871253, -24.34968618360933590, 0.1864209137778810865 ) ) ;
#62518=CARTESIAN_POINT ( 'NONE',  ( 18.81862293822770837, 7.596102252255398035, -1.500000000000002220 ) ) ;
#62520=CARTESIAN_POINT ( 'NONE',  ( -121.5228709571501042, -23.48783264082477018, -1.443836473390083253 ) ) ;
#62521=CARTESIAN_POINT ( 'NONE',  ( -31.62287095715005236, -29.50250243563736774, 8.947779886222150481 ) ) ;
#62524=CARTESIAN_POINT ( 'NONE',  ( -20.09103079077430820, 1.113595961413322177, -1.500000000000002220 ) ) ;
#62525=B_SPLINE_CURVE_WITH_KNOTS ( 'NONE', 3,
 ( #2151, #33084, #70642, #39184 ),
 .UNSPECIFIED., .F., .F.,
 ( 4, 4 ),
 ( 0.5501787936871235241, 0.5591852249592388358 ),
 .UNSPECIFIED. ) ;
#62526=CARTESIAN_POINT ( 'NONE',  ( -20.28541985502614509, -5.886007371444655689, 11.49999999999999645 ) ) ;
#62527=CARTESIAN_POINT ( 'NONE',  ( -7.320055889550622474, -20.87099576385019972, -1.500000000000002220 ) ) ;
#62528=CARTESIAN_POINT ( 'NONE',  ( -19.86366060283327784, 5.362777492974458049, 11.49999999999998934 ) ) ;
#62529=AXIS2_PLACEMENT_3D ( 'NONE', #32817, #63794, #95217 ) ;
#62530=B_SPLINE_CURVE_WITH_KNOTS ( 'NONE', 3,
 ( #53186, #59804, #90237, #45074 ),
 .UNSPECIFIED., .F., .F.,
 ( 4, 4 ),
 ( 0.000000000000000000, 9.999999999998897304E-05 ),
 .UNSPECIFIED. ) ;
#62531=CARTESIAN_POINT ( 'NONE',  ( -60.53843391936359097, -24.63355581998385446, 0.9682620441943891043 ) ) ;
#62532=VERTEX_POINT ( 'NONE', #54470 ) ;
#62533=CARTESIAN_POINT ( 'NONE',  ( -32.62287095715007013, -24.33832256527047377, 0.1851278514138576803 ) ) ;
#62534=ORIENTED_EDGE ( 'NONE', *, *, #43503, .F. ) ;
#62541=ORIENTED_EDGE ( 'NONE', *, *, #78076, .F. ) ;
#62542=DIRECTION ( 'NONE',  ( 0.000000000000000000, 0.9999999999976377785, 2.173523156925979975E-06 ) ) ;
#62543=DIRECTION ( 'NONE',  ( -3.773278334444167608E-23, 1.000000000000000000, 0.000000000000000000 ) ) ;
#62544=DIRECTION ( 'NONE',  ( 0.000000000000000000, 0.9999999999976377785, 2.173523156925979128E-06 ) ) ;
#62545=CARTESIAN_POINT ( 'NONE',  ( -12.00526669028610272, -16.82065764665920682, -1.500000000000002220 ) ) ;
#62546=ADVANCED_FACE ( 'NONE', ( #1184 ), #5310, .T. ) ;
#62547=AXIS2_PLACEMENT_3D ( 'NONE', #941, #70457, #31892 ) ;
#62548=CARTESIAN_POINT ( 'NONE',  ( 2.580163054138214562, 21.43444414123800712, 11.49999999999999645 ) ) ;
#62550=DIRECTION ( 'NONE',  ( -3.773278334453079030E-23, 0.9999999999976377785, 2.173523156925979128E-06 ) ) ;
#62552=CARTESIAN_POINT ( 'NONE',  ( -15.27869365379592281, -16.34152646814254339, -1.500000000000002220 ) ) ;
#62554=CARTESIAN_POINT ( 'NONE',  ( -47.59972437050590344, -23.96169478059712432, 10.65365249895718591 ) ) ;
#62555=CARTESIAN_POINT ( 'NONE',  ( -120.6228709571500417, -23.47596703998600631, 11.44779298504227683 ) ) ;
#62557=ORIENTED_EDGE ( 'NONE', *, *, #17189, .F. ) ;
#62559=CARTESIAN_POINT ( 'NONE',  ( -35.52841444253756009, -24.73531770709095312, 8.716586749053508498 ) ) ;
#62560=CARTESIAN_POINT ( 'NONE',  ( -12.67655569012464944, 16.65582705476778358, 11.49999999999998934 ) ) ;
#62564=B_SPLINE_CURVE_WITH_KNOTS ( 'NONE', 3,
 ( #8276, #77763, #85899, #17388 ),
 .UNSPECIFIED., .F., .F.,
 ( 4, 4 ),
 ( 0.000000000000000000, 9.999999999998897304E-05 ),
 .UNSPECIFIED. ) ;
#62565=EDGE_CURVE ( 'NONE', #91753, #20665, #36, .T. ) ;
#62566=FACE_OUTER_BOUND ( 'NONE', #92322, .T. ) ;
#62567=CARTESIAN_POINT ( 'NONE',  ( 6.572693220633653688, -20.11273663914708365, -1.500000000000002220 ) ) ;
#62568=VERTEX_POINT ( 'NONE', #178 ) ;
#62569=DIRECTION ( 'NONE',  ( 0.000000000000000000, -0.9999999999976377785, -2.173523156925979975E-06 ) ) ;
#62570=CARTESIAN_POINT ( 'NONE',  ( -18.25314811174894913, -11.95880190493418738, -1.500000000000002220 ) ) ;
#62571=CARTESIAN_POINT ( 'NONE',  ( -121.5228709571500758, -24.35013146730204525, 9.818937971375099494 ) ) ;
#62574=CARTESIAN_POINT ( 'NONE',  ( -0.2038501785326352067, 21.78777694363981254, -1.500000000000002220 ) ) ;
#62578=CARTESIAN_POINT ( 'NONE',  ( -48.52287095715006160, -29.50247984919015209, -1.443849546365058689 ) ) ;
#62579=VERTEX_POINT ( 'NONE', #39234 ) ;
#62581=VERTEX_POINT ( 'NONE', #70190 ) ;
#62582=VERTEX_POINT ( 'NONE', #16900 ) ;
#62583=CARTESIAN_POINT ( 'NONE',  ( -29.18684743162721418, -25.15141295360018603, 3.928745580597657661 ) ) ;
#62585=CARTESIAN_POINT ( 'NONE',  ( 20.46717832272283033, -5.532298862796615424, -1.500000000000002220 ) ) ;
#62586=CARTESIAN_POINT ( 'NONE',  ( -94.55479543721645541, -23.96119346886881019, -0.6495511937832051386 ) ) ;
#62587=CARTESIAN_POINT ( 'NONE',  ( -79.53726446675389639, -25.03138232695337706, 7.255560784353935588 ) ) ;
#62589=CARTESIAN_POINT ( 'NONE',  ( -58.52287095715006160, -29.50248528299804818, 1.056150453629034924 ) ) ;
#62591=CARTESIAN_POINT ( 'NONE',  ( 4.481524277812761525, 18.85844072219565604, -1.500000000000002220 ) ) ;
#62592=CARTESIAN_POINT ( 'NONE',  ( -51.82569660508215748, -25.29890250005943031, 5.651905355509026840 ) ) ;
#62593=VERTEX_POINT ( 'NONE', #79293 ) ;
#62594=CARTESIAN_POINT ( 'NONE',  ( -10.28394983263804185, -16.58134856480417341, 11.49999999999999645 ) ) ;
#62597=CARTESIAN_POINT ( 'NONE',  ( -79.90946178028013946, -25.14686779016199836, 6.961378012461956644 ) ) ;
#62598=ORIENTED_EDGE ( 'NONE', *, *, #82331, .T. ) ;
#62600=EDGE_CURVE ( 'NONE', #41185, #39688, #65109, .T. ) ;
#62602=ADVANCED_FACE ( 'NONE', ( #95028 ), #17404, .T. ) ;
#62604=CARTESIAN_POINT ( 'NONE',  ( -64.62287095715005592, -23.72747288104470087, -1.053458166803226348 ) ) ;
#62605=B_SPLINE_CURVE_WITH_KNOTS ( 'NONE', 3,
 ( #12695, #36041, #19805, #81722 ),
 .UNSPECIFIED., .F., .F.,
 ( 4, 4 ),
 ( 0.000000000000000000, 9.999999999998897304E-05 ),
 .UNSPECIFIED. ) ;
#62606=B_SPLINE_CURVE_WITH_KNOTS ( 'NONE', 3,
 ( #72099, #87812, #72595, #34026 ),
 .UNSPECIFIED., .F., .F.,
 ( 4, 4 ),
 ( 0.8994249224030640422, 0.9004256694438294018 ),
 .UNSPECIFIED. ) ;
#62607=CARTESIAN_POINT ( 'NONE',  ( -93.62801294614813230, -24.35071581493543391, 9.817618358456016381 ) ) ;
#62608=CARTESIAN_POINT ( 'NONE',  ( 16.91694316922610497, -9.995573847407506207, 11.49999999999998934 ) ) ;
#62609=CARTESIAN_POINT ( 'NONE',  ( -41.46379453422112249, -25.27805965137699218, 4.278542394115019576 ) ) ;
#62610=VERTEX_POINT ( 'NONE', #25517 ) ;
#62611=CARTESIAN_POINT ( 'NONE',  ( -19.30636564405121902, 9.640216152154000184, 11.49999999999998934 ) ) ;
#62612=CARTESIAN_POINT ( 'NONE',  ( -40.54156941310200324, -24.40034930558990922, 0.3402023900116037947 ) ) ;
#62613=CARTESIAN_POINT ( 'NONE',  ( -78.52287095715006160, -23.47593901973090169, -1.443836447538996648 ) ) ;
#62614=CARTESIAN_POINT ( 'NONE',  ( 22.67273400128462058, 4.441195646929153362, -1.500000000000002220 ) ) ;
#62617=PLANE ( 'NONE',  #64517 ) ;
#62618=CARTESIAN_POINT ( 'NONE',  ( -130.5728709571500588, -23.50395946778992595, -1.461890965025840927 ) ) ;
#62623=CARTESIAN_POINT ( 'NONE',  ( -110.0874522194761056, -25.18851129330323602, 3.319341060603216764 ) ) ;
#62624=CARTESIAN_POINT ( 'NONE',  ( -129.6237315874382432, -23.96119346886881019, -0.6495511937831975890 ) ) ;
#62625=CARTESIAN_POINT ( 'NONE',  ( -111.3439979973304332, -25.18425758082677746, 4.101024256656019773 ) ) ;
#62626=CARTESIAN_POINT ( 'NONE',  ( -19.25010300378637851, 5.133817055790010464, -1.500000000000002220 ) ) ;
#62627=ADVANCED_FACE ( 'NONE', ( #66110 ), #48364, .F. ) ;
#62628=CARTESIAN_POINT ( 'NONE',  ( -113.6228709571500559, -24.64898659630368627, 1.056161002820831474 ) ) ;
#62629=CARTESIAN_POINT ( 'NONE',  ( 4.927431051831622000, -19.18327824014073357, -1.500000000000002220 ) ) ;
#62630=VECTOR ( 'NONE', #35430, 1000.000000000000114 ) ;
#62631=CARTESIAN_POINT ( 'NONE',  ( -56.56717033891496982, -23.48783264082477018, -1.443836473390095909 ) ) ;
#62632=B_SPLINE_CURVE_WITH_KNOTS ( 'NONE', 3,
 ( #8210, #7702, #14801, #16313 ),
 .UNSPECIFIED., .F., .F.,
 ( 4, 4 ),
 ( 0.000000000000000000, 9.999999999998206125E-05 ),
 .UNSPECIFIED. ) ;
#62635=CARTESIAN_POINT ( 'NONE',  ( 8.056674255711671506, 19.11000797562349618, 11.49999999999999645 ) ) ;
#62636=DIRECTION ( 'NONE',  ( 1.000000000000000000, 3.773278334444167608E-23, 8.201307833595939069E-29 ) ) ;
#62638=CARTESIAN_POINT ( 'NONE',  ( -88.62287095715002749, -23.72747288104441665, -1.053458166803660889 ) ) ;
#62639=CARTESIAN_POINT ( 'NONE',  ( 18.68554041145753786, -12.99315341008173519, 11.49999999999999645 ) ) ;
#62640=ORIENTED_EDGE ( 'NONE', *, *, #49595, .F. ) ;
#62641=CARTESIAN_POINT ( 'NONE',  ( -69.63557792188336748, -24.15543982623907127, -0.2315651400026648155 ) ) ;
#62642=ADVANCED_FACE ( 'NONE', ( #56491 ), #96525, .T. ) ;
#62644=ORIENTED_EDGE ( 'NONE', *, *, #81316, .T. ) ;
#62645=B_SPLINE_CURVE_WITH_KNOTS ( 'NONE', 3,
 ( #43559, #66908, #26830, #97829 ),
 .UNSPECIFIED., .F., .F.,
 ( 4, 4 ),
 ( 0.000000000000000000, 9.999999999997510880E-05 ),
 .UNSPECIFIED. ) ;
#62646=CARTESIAN_POINT ( 'NONE',  ( -9.470923242388245455, -17.85692771776473364, -1.500000000000002220 ) ) ;
#62647=FACE_OUTER_BOUND ( 'NONE', #20479, .T. ) ;
#62652=EDGE_CURVE ( 'NONE', #80103, #39944, #72769, .T. ) ;
#62654=LINE ( 'NONE', #40798, #77627 ) ;
#62655=CARTESIAN_POINT ( 'NONE',  ( 10.67403711042701353, -20.27515232684288549, -1.500000000000002220 ) ) ;
#62656=CARTESIAN_POINT ( 'NONE',  ( -41.15328318997018897, -25.14988170789391830, 3.000103590172058077 ) ) ;
#62658=CARTESIAN_POINT ( 'NONE',  ( -0.6006773669993965559, 21.62980403441659760, -1.500000000000002220 ) ) ;
#62659=CARTESIAN_POINT ( 'NONE',  ( -104.6228709571500985, -24.34917612406837861, 0.1852690917426659811 ) ) ;
#62660=CARTESIAN_POINT ( 'NONE',  ( 13.94627346685978075, -15.57361473980792255, 11.49999999999999645 ) ) ;
#62661=ORIENTED_EDGE ( 'NONE', *, *, #30809, .F. ) ;
#62663=CARTESIAN_POINT ( 'NONE',  ( -103.5228709571500758, -24.64965694238408034, 8.947790433994194714 ) ) ;
#62664=CARTESIAN_POINT ( 'NONE',  ( -18.71521858236628333, -11.60751834597489740, -1.500000000000002220 ) ) ;
#62666=CARTESIAN_POINT ( 'NONE',  ( -30.57287095715006231, -23.48210175247266562, -1.443836490256470428 ) ) ;
#62668=CARTESIAN_POINT ( 'NONE',  ( -49.68454138742491466, -25.18440160747184464, 3.564592644700640189 ) ) ;
#62672=ORIENTED_EDGE ( 'NONE', *, *, #66531, .F. ) ;
#62673=B_SPLINE_CURVE_WITH_KNOTS ( 'NONE', 3,
 ( #10984, #96711, #41949, #41437 ),
 .UNSPECIFIED., .F., .F.,
 ( 4, 4 ),
 ( 0.05879740816001716858, 0.05979815520078245183 ),
 .UNSPECIFIED. ) ;
#62675=CARTESIAN_POINT ( 'NONE',  ( -71.55402431509982364, -23.96169478059713498, 10.65365249895718058 ) ) ;
#62676=CARTESIAN_POINT ( 'NONE',  ( -101.7453191491394477, -25.10936024163003211, 3.852396405368743171 ) ) ;
#62678=CARTESIAN_POINT ( 'NONE',  ( -20.44062828730913139, -1.133067592104922694, -1.500000000000002220 ) ) ;
#62680=CARTESIAN_POINT ( 'NONE',  ( -71.62287095715005592, -24.66019654487199020, 8.947790411086131712 ) ) ;
#62682=CARTESIAN_POINT ( 'NONE',  ( -56.62287095715007013, -24.50216790748205042, 0.6166512839542496183 ) ) ;
#62683=CARTESIAN_POINT ( 'NONE',  ( 21.78807519107708401, 4.755904613692067073, 11.49999999999998934 ) ) ;
#62687=ORIENTED_EDGE ( 'NONE', *, *, #64019, .F. ) ;
#62688=CARTESIAN_POINT ( 'NONE',  ( -29.78660512628383472, -25.21957512536681989, 4.203493191755291569 ) ) ;
#62690=B_SPLINE_CURVE_WITH_KNOTS ( 'NONE', 3,
 ( #71458, #26271, #25770, #17657, #1445, #41502 ),
 .UNSPECIFIED., .F., .F.,
 ( 4, 2, 4 ),
 ( 0.000000000000000000, 0.001380901958385383774, 0.002761803916770767548 ),
 .UNSPECIFIED. ) ;
#62691=CARTESIAN_POINT ( 'NONE',  ( -19.76906661924035191, -6.534152953431121347, -1.500000000000002220 ) ) ;
#62692=ORIENTED_EDGE ( 'NONE', *, *, #39127, .F. ) ;
#62695=AXIS2_PLACEMENT_3D ( 'NONE', #74864, #5368, #44439 ) ;
#62698=CARTESIAN_POINT ( 'NONE',  ( -0.6469382494902750080, 20.97623560764392181, -1.500000000000002220 ) ) ;
#62699=ORIENTED_EDGE ( 'NONE', *, *, #29102, .F. ) ;
#62701=CARTESIAN_POINT ( 'NONE',  ( -110.6228709571500701, -24.51163499207180152, 0.6490370598555511572 ) ) ;
#62704=VECTOR ( 'NONE', #36731, 1000.000000000000114 ) ;
#62706=CARTESIAN_POINT ( 'NONE',  ( -59.57900456839059444, -24.65952944569304961, 1.056160979905697905 ) ) ;
#62708=CARTESIAN_POINT ( 'NONE',  ( 17.07819277939130842, -14.19623557145530057, 11.49999999999999645 ) ) ;
#62709=ORIENTED_EDGE ( 'NONE', *, *, #73518, .F. ) ;
#62711=CARTESIAN_POINT ( 'NONE',  ( -38.62287095715005592, -24.65952944569303895, 1.056160979905692798 ) ) ;
#62712=ORIENTED_EDGE ( 'NONE', *, *, #31679, .F. ) ;
#62713=B_SPLINE_CURVE_WITH_KNOTS ( 'NONE', 3,
 ( #43283, #28051, #83822, #29529 ),
 .UNSPECIFIED., .F., .F.,
 ( 4, 4 ),
 ( 0.000000000000000000, 0.0001000000000000167422 ),
 .UNSPECIFIED. ) ;
#62714=CARTESIAN_POINT ( 'NONE',  ( -5.639450322166912777, -21.95568564230989850, -1.500000000000002220 ) ) ;
#62715=VECTOR ( 'NONE', #79179, 1000.000000000000114 ) ;
#62716=CARTESIAN_POINT ( 'NONE',  ( -76.62287095715007013, -24.64898659630367916, 1.056161002820826145 ) ) ;
#62718=ORIENTED_EDGE ( 'NONE', *, *, #22910, .T. ) ;
#62721=CARTESIAN_POINT ( 'NONE',  ( 5.670567493371958534, -19.34269084982597775, -1.500000000000002220 ) ) ;
#62722=DIRECTION ( 'NONE',  ( -3.773278334453079030E-23, 0.9999999999976377785, 2.173523156925979128E-06 ) ) ;
#62725=CARTESIAN_POINT ( 'NONE',  ( 21.16571772479873204, -7.350578744355993344, -1.500000000000002220 ) ) ;
#62726=VERTEX_POINT ( 'NONE', #55987 ) ;
#62727=VERTEX_POINT ( 'NONE', #35139 ) ;
#62728=CARTESIAN_POINT ( 'NONE',  ( -101.2523990460597503, -25.16257427658810641, 6.807414179791832609 ) ) ;
#62730=CARTESIAN_POINT ( 'NONE',  ( -39.93645079509425244, -25.31561181395491289, 4.983313389499331336 ) ) ;
#62733=EDGE_CURVE ( 'NONE', #38686, #1347, #64107, .T. ) ;
#62736=CARTESIAN_POINT ( 'NONE',  ( -130.5728709571500588, -24.47827083238276202, 0.5637492489085990099 ) ) ;
#62737=CARTESIAN_POINT ( 'NONE',  ( -1.979602623192304955, -19.45764201480039901, -1.500000000000002220 ) ) ;
#62738=CARTESIAN_POINT ( 'NONE',  ( -39.52287095715006870, -23.47596703998600631, 11.44779298504229281 ) ) ;
#62739=VERTEX_POINT ( 'NONE', #33635 ) ;
#62741=CARTESIAN_POINT ( 'NONE',  ( 3.930203739357332360, 21.12693704021120666, -1.500000000000002220 ) ) ;
#62743=CARTESIAN_POINT ( 'NONE',  ( -62.52287095715006160, -23.73934037231757088, 11.05740245334329153 ) ) ;
#62744=CARTESIAN_POINT ( 'NONE',  ( -38.62287095715005592, -23.47593901973091235, -1.443836447539011525 ) ) ;
#62745=CARTESIAN_POINT ( 'NONE',  ( -59.58953762381671027, -23.48783264082478794, -1.443836473390069042 ) ) ;
#62746=CARTESIAN_POINT ( 'NONE',  ( -111.6228709571500559, -23.48783264082479505, -1.443836473390060604 ) ) ;
#62747=CARTESIAN_POINT ( 'NONE',  ( -21.29394331855728240, -8.360804490491451801, -1.500000000000002220 ) ) ;
#62749=CARTESIAN_POINT ( 'NONE',  ( -101.5228709571500758, -23.47593901973090524, -1.443836447538996426 ) ) ;
#62750=CARTESIAN_POINT ( 'NONE',  ( -92.62287095715005592, -24.33832256527048088, 0.1851278514138620102 ) ) ;
#62751=CARTESIAN_POINT ( 'NONE',  ( -17.62595516807937557, -9.487554784798948759, 11.49999999999999645 ) ) ;
#62752=CARTESIAN_POINT ( 'NONE',  ( -80.30894842687054336, -25.31594316168605374, 4.506568925094878608 ) ) ;
#62753=CARTESIAN_POINT ( 'NONE',  ( -87.52287095715006160, -24.64965694238575011, 8.947790433994196491 ) ) ;
#62754=LINE ( 'NONE', #54628, #79790 ) ;
#62755=CARTESIAN_POINT ( 'NONE',  ( -37.52287095715006870, -29.50250786944525672, 11.44777988621624232 ) ) ;
#62756=ORIENTED_EDGE ( 'NONE', *, *, #75076, .T. ) ;
#62759=CARTESIAN_POINT ( 'NONE',  ( 21.64095104908334122, -2.195182070091274529, -1.500000000000002220 ) ) ;
#62761=CARTESIAN_POINT ( 'NONE',  ( -3.718233408413001762, 19.32670252783854536, -1.500000000000002220 ) ) ;
#62763=CARTESIAN_POINT ( 'NONE',  ( -122.6228709571500843, -23.96127896941633750, -0.6493128931037740470 ) ) ;
#62764=ADVANCED_FACE ( 'NONE', ( #68078 ), #90386, .T. ) ;
#62765=CARTESIAN_POINT ( 'NONE',  ( -109.5056412146432052, -25.27925783859062037, 4.749485557442086225 ) ) ;
#62768=CARTESIAN_POINT ( 'NONE',  ( -73.62287095715008434, -24.35013146730204525, 9.818937971375108376 ) ) ;
#62769=CARTESIAN_POINT ( 'NONE',  ( 11.66944253441096002, 16.90307425063352298, 11.49999999999999645 ) ) ;
#62771=EDGE_CURVE ( 'NONE', #65202, #27379, #97026, .T. ) ;
#62773=CARTESIAN_POINT ( 'NONE',  ( -120.6249283607330085, -24.63355581998386157, 0.9682620441943888823 ) ) ;
#62774=CARTESIAN_POINT ( 'NONE',  ( 1.383477600506065164, -22.57338898373578218, 11.49999999999999645 ) ) ;
#62776=CARTESIAN_POINT ( 'NONE',  ( -83.52287095715006160, -23.47596703998600631, 11.44779298504228571 ) ) ;
#62777=CARTESIAN_POINT ( 'NONE',  ( -26.71433665274188130, -24.81880000428164124, 7.190069475304298408 ) ) ;
#62778=CARTESIAN_POINT ( 'NONE',  ( -97.63857696127199404, -23.48783264082477018, -1.443836473390088360 ) ) ;
#62781=CARTESIAN_POINT ( 'NONE',  ( -25.53098197642538736, -24.61459394604217010, 4.942812361920813302 ) ) ;
#62782=EDGE_CURVE ( 'NONE', #6498, #28719, #44744, .T. ) ;
#62784=EDGE_CURVE ( 'NONE', #33865, #62952, #75080, .T. ) ;
#62786=CARTESIAN_POINT ( 'NONE',  ( -79.51137944035450289, -25.31596313913097873, 5.389239573282282869 ) ) ;
#62787=CARTESIAN_POINT ( 'NONE',  ( 7.682656365740156090, -21.48159684637525046, -1.500000000000002220 ) ) ;
#62788=CARTESIAN_POINT ( 'NONE',  ( -74.62680018750160116, -24.51314013834315375, 0.6176544820404124003 ) ) ;
#62789=CARTESIAN_POINT ( 'NONE',  ( -96.58652322487247943, -24.51314013834316086, 0.6176544820404182845 ) ) ;
#62790=CARTESIAN_POINT ( 'NONE',  ( -119.5895376238167245, -24.64898659630368627, 1.056161002820393602 ) ) ;
#62791=CARTESIAN_POINT ( 'NONE',  ( 15.70178742502441693, -15.98865493379879332, 11.49999999999999645 ) ) ;
#62792=ORIENTED_EDGE ( 'NONE', *, *, #46281, .F. ) ;
#62793=CARTESIAN_POINT ( 'NONE',  ( -70.62287095715001328, -24.63345952396257488, 9.038047939301510070 ) ) ;
#62795=CARTESIAN_POINT ( 'NONE',  ( -21.91604229967229500, -0.6759211909499470705, 11.49999999999998934 ) ) ;
#62797=B_SPLINE_CURVE_WITH_KNOTS ( 'NONE', 3,
 ( #50930, #60543, #28087, #6231 ),
 .UNSPECIFIED., .F., .F.,
 ( 4, 4 ),
 ( 3.895932028743765719E-09, 0.001954337564626884745 ),
 .UNSPECIFIED. ) ;
#62798=CARTESIAN_POINT ( 'NONE',  ( -44.62857276611402568, -24.51419770103159834, 9.386484678747169852 ) ) ;
#62799=PLANE ( 'NONE',  #53561 ) ;
#62800=ORIENTED_EDGE ( 'NONE', *, *, #87319, .T. ) ;
#62804=CARTESIAN_POINT ( 'NONE',  ( -20.46784169311667867, 0.4426517378232717737, 11.49999999999998934 ) ) ;
#62805=ORIENTED_EDGE ( 'NONE', *, *, #100198, .F. ) ;
#62806=ORIENTED_EDGE ( 'NONE', *, *, #98727, .T. ) ;
#62807=VERTEX_POINT ( 'NONE', #75665 ) ;
#62808=ORIENTED_EDGE ( 'NONE', *, *, #22368, .F. ) ;
#62809=CARTESIAN_POINT ( 'NONE',  ( -3.381418692465893105, -22.81955385325859709, 11.49999999999998934 ) ) ;
#62810=CARTESIAN_POINT ( 'NONE',  ( -40.11496927896248366, -25.30524842186639844, 5.093185296294494790 ) ) ;
#62811=CARTESIAN_POINT ( 'NONE',  ( 11.02309159617336221, -17.05227643984133934, -1.500000000000002220 ) ) ;
#62812=VERTEX_POINT ( 'NONE', #6166 ) ;
#62816=CARTESIAN_POINT ( 'NONE',  ( -113.2228709571500502, -23.47593901973090524, -1.443836447538996426 ) ) ;
#62817=CARTESIAN_POINT ( 'NONE',  ( -97.92287095715008149, -23.47596703998600276, 11.44779298504227860 ) ) ;
#62818=CARTESIAN_POINT ( 'NONE',  ( -17.67684169981329845, 12.20363403927300183, 11.49999999999999645 ) ) ;
#62820=CARTESIAN_POINT ( 'NONE',  ( -125.5562042904833930, -24.99132157543167310, 2.256160258750667946 ) ) ;
#62821=CARTESIAN_POINT ( 'NONE',  ( -34.62287095715005592, -24.33832256527048088, 0.1851278514138579023 ) ) ;
#62822=ORIENTED_EDGE ( 'NONE', *, *, #65079, .F. ) ;
#62824=CARTESIAN_POINT ( 'NONE',  ( -2.856624844580134770, 20.53689577262001364, -1.500000000000002220 ) ) ;
#62825=ORIENTED_EDGE ( 'NONE', *, *, #6706, .T. ) ;
#62826=CARTESIAN_POINT ( 'NONE',  ( -125.5222534793145854, -23.48783264082478794, -1.443836473390061936 ) ) ;
#62827=ORIENTED_EDGE ( 'NONE', *, *, #24045, .T. ) ;
#62828=B_SPLINE_SURFACE_WITH_KNOTS ( 'NONE', 3, 3, ( 
 ( #30029, #60514, #61003, #68608 ),
 ( #91937, #4717, #67621, #98041 ),
 ( #91427, #89944, #21907, #29035 ),
 ( #51391, #35668, #74707, #76203 ),
 ( #82329, #43779, #37652, #5206 ),
 ( #20919, #70106, #23402, #46773 ),
 ( #47275, #9199, #71115, #38143 ) ),
 .UNSPECIFIED., .F., .F., .F.,
 ( 4, 3, 4 ),
 ( 4, 4 ),
 ( 0.0004766839783846337159, 0.1029713700210910243, 0.2054660560637974198 ),
 ( 0.2295523914546782895, 0.2306710310623432680 ),
 .UNSPECIFIED. ) ;
#62829=CARTESIAN_POINT ( 'NONE',  ( -41.54628241281430689, -24.15620529776627734, 10.23563542870660825 ) ) ;
#62830=DIRECTION ( 'NONE',  ( -3.773278334453079030E-23, 0.9999999999976377785, 2.173523156925979128E-06 ) ) ;
#62832=ORIENTED_EDGE ( 'NONE', *, *, #30542, .F. ) ;
#62833=CARTESIAN_POINT ( 'NONE',  ( -109.5228709571500616, -23.47596703998600631, 11.44779298504228038 ) ) ;
#62834=CARTESIAN_POINT ( 'NONE',  ( -42.52203033503141683, -23.48786465467240347, 11.44779295918255535 ) ) ;
#62835=CARTESIAN_POINT ( 'NONE',  ( -78.52287095715000476, -23.94994826722564696, -0.6494450866342719175 ) ) ;
#62836=CARTESIAN_POINT ( 'NONE',  ( -7.037580251249667462, -20.86201633182841420, 11.49999999999999645 ) ) ;
#62838=CARTESIAN_POINT ( 'NONE',  ( -14.53490578827140212, -17.26895500059623956, 11.49999999999998934 ) ) ;
#62840=CARTESIAN_POINT ( 'NONE',  ( 3.785439364192078937, -20.66625369722972749, 11.49999999999998934 ) ) ;
#62843=EDGE_LOOP ( 'NONE', ( #92793, #45476, #88759, #46176 ) ) ;
#62845=CARTESIAN_POINT ( 'NONE',  ( -80.62287095715005592, -23.84047902841602351, -0.8780736468305712084 ) ) ;
#62846=VECTOR ( 'NONE', #22436, 1000.000000000000114 ) ;
#62849=EDGE_LOOP ( 'NONE', ( #37728, #15466, #50089, #63192 ) ) ;
#62850=CARTESIAN_POINT ( 'NONE',  ( 16.66693084842116335, 13.01107939256401913, -1.500000000000002220 ) ) ;
#62852=ADVANCED_FACE ( 'NONE', ( #43745 ), #44221, .T. ) ;
#62853=CARTESIAN_POINT ( 'NONE',  ( -60.72545834919631602, -25.33009847151395633, 4.495758292450051208 ) ) ;
#62854=CARTESIAN_POINT ( 'NONE',  ( -41.52287095715006870, -29.50250243563736774, 8.947779886222148704 ) ) ;
#62857=B_SPLINE_CURVE_WITH_KNOTS ( 'NONE', 3,
 ( #13840, #51428, #82363, #76234 ),
 .UNSPECIFIED., .F., .F.,
 ( 4, 4 ),
 ( 0.000000000000000000, 0.0001000000000000028644 ),
 .UNSPECIFIED. ) ;
#62858=CARTESIAN_POINT ( 'NONE',  ( -2.516727866726558460, 22.04588476715296963, -1.500000000000002220 ) ) ;
#62861=ADVANCED_FACE ( 'NONE', ( #46232 ), #45734, .T. ) ;
#62863=CARTESIAN_POINT ( 'NONE',  ( -51.72290159494567519, -25.31633202804502147, 5.484617888210121528 ) ) ;
#62864=CARTESIAN_POINT ( 'NONE',  ( -48.62287095715003460, -24.33832256526968862, 0.1851278514119848728 ) ) ;
#62865=CARTESIAN_POINT ( 'NONE',  ( -126.5899062329566505, -24.15543982623907482, -0.2315651400026573492 ) ) ;
#62867=CARTESIAN_POINT ( 'NONE',  ( -85.52287095715004739, -24.99156044556120193, 7.747789690856173195 ) ) ;
#62868=LINE ( 'NONE', #55247, #4847 ) ;
#62869=CARTESIAN_POINT ( 'NONE',  ( 13.74000504945409418, 13.82049530813991467, 11.49999999999998934 ) ) ;
#62870=CARTESIAN_POINT ( 'NONE',  ( -21.38522110535750542, 1.317000383210971792, -1.500000000000002220 ) ) ;
#62871=CARTESIAN_POINT ( 'NONE',  ( -62.65462279266101575, -23.48783264082476308, -1.443836473390090580 ) ) ;
#62872=CARTESIAN_POINT ( 'NONE',  ( -60.55142834745385727, -24.15602025861357660, 10.28564288302606933 ) ) ;
#62875=CARTESIAN_POINT ( 'NONE',  ( -20.89466310375201985, -8.809181082428260368, -1.500000000000002220 ) ) ;
#62877=CARTESIAN_POINT ( 'NONE',  ( -98.59358066329336623, -23.96119346886881019, -0.6495511937832081362 ) ) ;
#62879=CARTESIAN_POINT ( 'NONE',  ( -17.31707178780640533, -9.736581320607820444, 11.49999999999999645 ) ) ;
#62880=CARTESIAN_POINT ( 'NONE',  ( -123.5194348897975516, -24.51419770103158768, 9.386484678747160970 ) ) ;
#62886=CARTESIAN_POINT ( 'NONE',  ( -51.70072539166533687, -25.10936008140465248, 3.987152415576288522 ) ) ;
#62887=CARTESIAN_POINT ( 'NONE',  ( -18.45943378446990835, 11.37049804852326140, -1.500000000000002220 ) ) ;
#62889=FACE_OUTER_BOUND ( 'NONE', #50758, .T. ) ;
#62890=CARTESIAN_POINT ( 'NONE',  ( 16.53150372360616771, 10.32350692489952593, -1.500000000000002220 ) ) ;
#62891=CARTESIAN_POINT ( 'NONE',  ( -95.52287095715006160, -29.50249982740957577, 7.747779886224967605 ) ) ;
#62893=CARTESIAN_POINT ( 'NONE',  ( -13.40315722217803973, 15.35114911505495172, 11.49999999999999645 ) ) ;
#62894=CARTESIAN_POINT ( 'NONE',  ( -62.62287095715004881, -24.64898659630528854, 1.056161002820822592 ) ) ;
#62895=DIRECTION ( 'NONE',  ( -3.773278334453079618E-23, 0.9999999999976377785, 2.173523156925979975E-06 ) ) ;
#62897=CARTESIAN_POINT ( 'NONE',  ( -79.01456066750945695, -25.21459190771157566, 6.490408043050610587 ) ) ;
#62899=CARTESIAN_POINT ( 'NONE',  ( -48.90136019426822145, -25.31602018323131986, 5.866402636874745724 ) ) ;
#62900=CARTESIAN_POINT ( 'NONE',  ( -40.63662915703572054, -24.63419186844611630, 9.035850630976923981 ) ) ;
#62902=CARTESIAN_POINT ( 'NONE',  ( 19.44710440357065551, 5.058846670610233076, 11.49999999999998934 ) ) ;
#62903=CARTESIAN_POINT ( 'NONE',  ( -109.6310386362097518, -23.73766607897670156, -1.055555164236452681 ) ) ;
#62904=VERTEX_POINT ( 'NONE', #62981 ) ;
#62906=AXIS2_PLACEMENT_3D ( 'NONE', #33781, #3354, #71853 ) ;
#62907=ADVANCED_FACE ( 'NONE', ( #7669 ), #76658, .T. ) ;
#62908=CARTESIAN_POINT ( 'NONE',  ( -18.82434810282327220, -12.99595988342530362, 11.49999999999999645 ) ) ;
#62909=CARTESIAN_POINT ( 'NONE',  ( 1.118074629359579797, -22.68859683979520980, -1.500000000000002220 ) ) ;
#62911=CARTESIAN_POINT ( 'NONE',  ( -53.62287095715003460, -24.51387760970723662, 9.387446482453425389 ) ) ;
#62914=CARTESIAN_POINT ( 'NONE',  ( -49.52287095715009002, -23.96127896941631619, -0.6493128931038038010 ) ) ;
#62915=EDGE_CURVE ( 'NONE', #26478, #45688, #66671, .T. ) ;
#62917=CARTESIAN_POINT ( 'NONE',  ( -128.5220659786135116, -23.73791477778912551, 11.05961554403169522 ) ) ;
#62919=EDGE_LOOP ( 'NONE', ( #99972, #98419, #28982, #70049 ) ) ;
#62921=CARTESIAN_POINT ( 'NONE',  ( -16.54958403137900191, 11.88860064210666856, 11.49999999999998934 ) ) ;
#62923=CARTESIAN_POINT ( 'NONE',  ( -5.582908757718670678, 22.30220962497079285, 11.49999999999998934 ) ) ;
#62925=FACE_OUTER_BOUND ( 'NONE', #11620, .T. ) ;
#62927=B_SPLINE_CURVE_WITH_KNOTS ( 'NONE', 3,
 ( #40177, #72638, #33565, #40681, #56919, #24939, #10225, #79224, #94458, #33067, #80741, #71128, #1624, #39665 ),
 .UNSPECIFIED., .F., .F.,
 ( 4, 2, 2, 2, 2, 2, 4 ),
 ( 0.000000000000000000, 0.0001567136917012794807, 0.0003134273834025589614, 0.0004701410751038384420, 0.0006268547668051179227, 0.0009402821502076935808, 0.001253709533610269239 ),
 .UNSPECIFIED. ) ;
#62928=CARTESIAN_POINT ( 'NONE',  ( -97.52287095715003318, -24.66019654487200441, 8.947790411086119278 ) ) ;
#62931=CARTESIAN_POINT ( 'NONE',  ( 11.00477826368897283, 18.22718707545001138, 11.49999999999999645 ) ) ;
#62934=CARTESIAN_POINT ( 'NONE',  ( -17.05807961832342912, 14.25954964135033265, -1.500000000000002220 ) ) ;
#62935=CARTESIAN_POINT ( 'NONE',  ( -6.358105417860958397, -19.66046682221446318, 11.49999999999998934 ) ) ;
#62936=VERTEX_POINT ( 'NONE', #39115 ) ;
#62938=CARTESIAN_POINT ( 'NONE',  ( -69.85508590344461766, -25.32724624944561853, 4.398071659717722959 ) ) ;
#62939=ORIENTED_EDGE ( 'NONE', *, *, #39135, .F. ) ;
#62940=DIRECTION ( 'NONE',  ( -3.773278334453079618E-23, 0.9999999999976377785, 2.173523156925979975E-06 ) ) ;
#62941=ORIENTED_EDGE ( 'NONE', *, *, #6288, .T. ) ;
#62944=CARTESIAN_POINT ( 'NONE',  ( -17.86878485216894319, -10.78119150571587781, -1.500000000000002220 ) ) ;
#62945=CARTESIAN_POINT ( 'NONE',  ( 17.39636294008568740, -13.23181597624684791, 11.49999999999999645 ) ) ;
#62946=CARTESIAN_POINT ( 'NONE',  ( -102.6228709571500417, -23.73934037231757443, 11.05740245334328087 ) ) ;
#62947=CARTESIAN_POINT ( 'NONE',  ( -78.55425796183220655, -23.96169478059713498, 10.65365249895717881 ) ) ;
#62948=CARTESIAN_POINT ( 'NONE',  ( 8.471766090126642723, -20.80389698432254519, 11.49999999999998934 ) ) ;
#62949=CARTESIAN_POINT ( 'NONE',  ( -118.6289526454650058, -23.48786465467241769, 11.44779295918253581 ) ) ;
#62950=CARTESIAN_POINT ( 'NONE',  ( -71.70841769935766763, -25.25720466352798255, 6.192981421160952848 ) ) ;
#62951=CARTESIAN_POINT ( 'NONE',  ( -31.58953762381672092, -24.64965694238574656, 8.947790433994208925 ) ) ;
#62952=VERTEX_POINT ( 'NONE', #9168 ) ;
#62953=B_SPLINE_SURFACE_WITH_KNOTS ( 'NONE', 3, 1, ( 
 ( #10430, #12428 ),
 ( #41391, #43396 ),
 ( #96668, #72847 ),
 ( #66248, #34284 ),
 ( #19042, #80951 ),
 ( #81456, #42413 ),
 ( #80448, #95675 ),
 ( #20045, #66749 ),
 ( #4333, #4825 ),
 ( #35778, #27667 ),
 ( #50016, #18545 ) ),
 .UNSPECIFIED., .F., .F., .F.,
 ( 4, 1, 1, 1, 1, 1, 1, 1, 4 ),
 ( 2, 2 ),
 ( 0.000000000000000000, 0.1022030370352139811, 0.2110233423738757941, 0.3250996615652070321, 0.4465020971348850898, 0.5737877176488546116, 0.7089007097660665613, 0.8503578712933955730, 1.000000000000000000 ),
 ( 0.000000000000000000, 1.000000000000000000 ),
 .UNSPECIFIED. ) ;
#62954=EDGE_LOOP ( 'NONE', ( #32697, #68774, #11018, #37145 ) ) ;
#62955=ORIENTED_EDGE ( 'NONE', *, *, #48299, .T. ) ;
#62956=ORIENTED_EDGE ( 'NONE', *, *, #43262, .T. ) ;
#62957=CARTESIAN_POINT ( 'NONE',  ( -8.434714792116727367, -19.68496499552307455, -1.500000000000002220 ) ) ;
#62958=CARTESIAN_POINT ( 'NONE',  ( 15.34105849444754455, 16.31744944422920440, 11.49999999999999645 ) ) ;
#62960=CARTESIAN_POINT ( 'NONE',  ( -5.931750313267273533, -20.21149935180699231, 11.49999999999998934 ) ) ;
#62961=FACE_OUTER_BOUND ( 'NONE', #23615, .T. ) ;
#62962=ADVANCED_FACE ( 'NONE', ( #70068 ), #24392, .F. ) ;
#62963=CARTESIAN_POINT ( 'NONE',  ( 0.05828707793547563409, -19.95834144014285272, -1.500000000000002220 ) ) ;
#62964=DIRECTION ( 'NONE',  ( -3.773278334444166432E-23, 1.000000000000000000, 0.000000000000000000 ) ) ;
#62965=CARTESIAN_POINT ( 'NONE',  ( -43.52287095715007581, -24.66019654487199375, 8.947790411086128159 ) ) ;
#62966=CARTESIAN_POINT ( 'NONE',  ( -16.59477544326466969, -14.39948450415919723, -1.500000000000002220 ) ) ;
#62967=PLANE ( 'NONE',  #75485 ) ;
#62970=B_SPLINE_CURVE_WITH_KNOTS ( 'NONE', 3,
 ( #10928, #2829, #49504, #93648, #56120, #64750, #24143, #71836, #41383, #62730, #56623, #16522, #95667, #25138, #31764, #64241 ),
 .UNSPECIFIED., .F., .F.,
 ( 4, 2, 2, 2, 2, 2, 2, 4 ),
 ( 0.000000000000000000, 0.0001831894960030059445, 0.0003663789920060118890, 0.0007327579840120237780, 0.0009159474800150220518, 0.001099136976018020434, 0.001282326472021018708, 0.001465515968024016982 ),
 .UNSPECIFIED. ) ;
#62971=EDGE_CURVE ( 'NONE', #69183, #72199, #7162, .T. ) ;
#62973=CARTESIAN_POINT ( 'NONE',  ( 20.80141654084381386, -1.409215765453083469, 11.49999999999999645 ) ) ;
#62975=EDGE_CURVE ( 'NONE', #62904, #6142, #17036, .T. ) ;
#62977=EDGE_CURVE ( 'NONE', #78888, #25133, #25486, .T. ) ;
#62978=CARTESIAN_POINT ( 'NONE',  ( -108.6228709571501128, -24.35013146730204525, 9.818937971375106599 ) ) ;
#62979=CARTESIAN_POINT ( 'NONE',  ( -90.62287095715004170, -25.00158670708908915, 2.256160236439166411 ) ) ;
#62980=CARTESIAN_POINT ( 'NONE',  ( 3.065528897535349628, -21.08962430476942274, 11.49999999999998934 ) ) ;
#62981=CARTESIAN_POINT ( 'NONE',  ( -46.62287095715004881, -23.48786465467241058, 11.44779295918255180 ) ) ;
#62982=EDGE_CURVE ( 'NONE', #84523, #88166, #67925, .T. ) ;
#62983=CARTESIAN_POINT ( 'NONE',  ( -66.52287095715006160, -23.47596703998600631, 11.44779298504228748 ) ) ;
#62984=CARTESIAN_POINT ( 'NONE',  ( -64.62738566448841482, -24.51419770103159124, 9.386484678747168076 ) ) ;
#62986=CARTESIAN_POINT ( 'NONE',  ( 6.936750662203477802, 21.44973376661030429, -1.500000000000002220 ) ) ;
#62988=ORIENTED_EDGE ( 'NONE', *, *, #77021, .F. ) ;
#62989=CARTESIAN_POINT ( 'NONE',  ( -35.62287095715005592, -25.00158670708908915, 2.256160236439166855 ) ) ;
#62990=CARTESIAN_POINT ( 'NONE',  ( -31.60165186599006049, -23.96169478059712432, 10.65365249895719124 ) ) ;
#62991=CARTESIAN_POINT ( 'NONE',  ( 8.085132396474181249, 17.94908993440701295, 11.49999999999999645 ) ) ;
#62992=FACE_OUTER_BOUND ( 'NONE', #95621, .T. ) ;
#62994=LINE ( 'NONE', #47758, #56115 ) ;
#62996=ORIENTED_EDGE ( 'NONE', *, *, #77588, .T. ) ;
#62997=CARTESIAN_POINT ( 'NONE',  ( -90.52287095715003318, -25.00182538069145366, 7.747789668545104647 ) ) ;
#63000=CARTESIAN_POINT ( 'NONE',  ( -68.58953762381672448, -24.64965694238406968, 8.947790433994660120 ) ) ;
#63001=CARTESIAN_POINT ( 'NONE',  ( 15.11087362536062173, -12.71848776332401521, 11.49999999999998934 ) ) ;
#63003=ORIENTED_EDGE ( 'NONE', *, *, #94937, .T. ) ;
#63004=CARTESIAN_POINT ( 'NONE',  ( -16.64171244834553676, 11.49637152377623828, 11.49999999999999645 ) ) ;
#63008=CARTESIAN_POINT ( 'NONE',  ( -53.62287095715004170, -24.50216790748098461, 0.6166512839513605959 ) ) ;
#63010=CARTESIAN_POINT ( 'NONE',  ( -51.04919692492541117, -25.30031294595708857, 5.371548930483984741 ) ) ;
#63011=CARTESIAN_POINT ( 'NONE',  ( -67.62287095715004170, -24.50216790748098816, 0.6166512839513741406 ) ) ;
#63013=FACE_OUTER_BOUND ( 'NONE', #6758, .T. ) ;
#63014=CARTESIAN_POINT ( 'NONE',  ( -14.99618758923778117, -13.25627519679515665, -1.500000000000002220 ) ) ;
#63015=ADVANCED_FACE ( 'NONE', ( #64496 ), #1574, .T. ) ;
#63016=CARTESIAN_POINT ( 'NONE',  ( -58.62287095715002039, -24.33832256526968862, 0.1851278514119840124 ) ) ;
#63018=EDGE_LOOP ( 'NONE', ( #54920, #44630, #7884, #40718 ) ) ;
#63019=EDGE_CURVE ( 'NONE', #33587, #58273, #40050, .T. ) ;
#63020=CARTESIAN_POINT ( 'NONE',  ( -79.59200941457424960, -24.15620529776628089, 10.23563542870660470 ) ) ;
#63021=CARTESIAN_POINT ( 'NONE',  ( -109.3750630267952317, -25.29012884606049383, 4.026263179138138248 ) ) ;
#63022=CARTESIAN_POINT ( 'NONE',  ( -89.62287095715004170, -24.64898659630529210, 1.056161002820827921 ) ) ;
#63024=CARTESIAN_POINT ( 'NONE',  ( -118.1692003789631684, -25.31326721218303888, 3.500953664922430431 ) ) ;
#63025=CARTESIAN_POINT ( 'NONE',  ( -83.62626469299168264, -24.51314013834315020, 0.6176544820404096248 ) ) ;
#63027=ADVANCED_FACE ( 'NONE', ( #42147 ), #3576, .T. ) ;
#63028=CARTESIAN_POINT ( 'NONE',  ( -101.9689938327708774, -25.25978491487772004, 3.590542621692357717 ) ) ;
#63029=EDGE_LOOP ( 'NONE', ( #23786, #63838, #3068, #49717 ) ) ;
#63032=CARTESIAN_POINT ( 'NONE',  ( -3.904290608643684379, -19.93223805144805283, -1.500000000000002220 ) ) ;
#63033=EDGE_CURVE ( 'NONE', #49913, #27337, #32511, .T. ) ;
#63035=CARTESIAN_POINT ( 'NONE',  ( -59.64293371994119752, -23.96169478059713143, 10.65365249895718769 ) ) ;
#63037=CARTESIAN_POINT ( 'NONE',  ( -94.52287095715006160, -23.47596703998600631, 11.44779298504228393 ) ) ;
#63038=CARTESIAN_POINT ( 'NONE',  ( -19.70923665959843873, 4.302044407003456250, -1.500000000000002220 ) ) ;
#63039=CARTESIAN_POINT ( 'NONE',  ( -20.67868931609407213, -4.308284118179648736, 11.49999999999999645 ) ) ;
#63041=CARTESIAN_POINT ( 'NONE',  ( 21.58644828898399481, -4.983269013152989757, -1.500000000000002220 ) ) ;
#63043=CARTESIAN_POINT ( 'NONE',  ( -12.99546161633903552, -15.93940442571882876, 11.49999999999998934 ) ) ;
#63044=CARTESIAN_POINT ( 'NONE',  ( -55.52287095715008292, -23.47593901973090169, -1.443836447538997092 ) ) ;
#63045=ORIENTED_EDGE ( 'NONE', *, *, #86469, .T. ) ;
#63050=EDGE_LOOP ( 'NONE', ( #21127, #33444, #22852, #98952 ) ) ;
#63054=PLANE ( 'NONE',  #16215 ) ;
#63055=CARTESIAN_POINT ( 'NONE',  ( -55.52287095715005449, -24.99156044556119483, 7.747789690856173195 ) ) ;
#63056=CARTESIAN_POINT ( 'NONE',  ( -68.59719453268294842, -23.96169478059712787, 10.65365249895718414 ) ) ;
#63057=CARTESIAN_POINT ( 'NONE',  ( 20.35908867758196550, 3.722869731652943770, -1.500000000000002220 ) ) ;
#63058=CARTESIAN_POINT ( 'NONE',  ( 12.90450488963236353, -17.39418326053592168, 11.49999999999999645 ) ) ;
#63061=CARTESIAN_POINT ( 'NONE',  ( -55.52287095715006870, -29.50247984919015209, -1.443849546365056913 ) ) ;
#63062=CARTESIAN_POINT ( 'NONE',  ( -9.622923231576368863, -20.19340101508991125, -1.500000000000002220 ) ) ;
#63063=CARTESIAN_POINT ( 'NONE',  ( -47.50043236403589475, -24.15620529776627379, 10.23563542870660825 ) ) ;
#63064=CARTESIAN_POINT ( 'NONE',  ( -84.50114960218334659, -24.65952944569303895, 1.056160979905700348 ) ) ;
#63066=CARTESIAN_POINT ( 'NONE',  ( -100.6814946224345846, -25.31267346029541443, 4.736250531364077254 ) ) ;
#63067=CARTESIAN_POINT ( 'NONE',  ( -52.58953762381673158, -24.64965694238406968, 8.947790433994663672 ) ) ;
#63068=EDGE_LOOP ( 'NONE', ( #31577, #7413, #24750, #24472 ) ) ;
#63069=CARTESIAN_POINT ( 'NONE',  ( -39.62287095715005592, -24.66019654487199020, 8.947790411086135265 ) ) ;
#63070=VERTEX_POINT ( 'NONE', #63486 ) ;
#63071=VECTOR ( 'NONE', #18056, 1000.000000000000114 ) ;
#63073=CARTESIAN_POINT ( 'NONE',  ( -19.86647519178106691, -7.318714840676754818, -1.500000000000002220 ) ) ;
#63074=VERTEX_POINT ( 'NONE', #25899 ) ;
#63075=CARTESIAN_POINT ( 'NONE',  ( -50.53277973184150795, -24.73486907724918282, 1.287355809206963464 ) ) ;
#63076=CARTESIAN_POINT ( 'NONE',  ( 11.26692973276593968, -18.67385317477220497, -1.500000000000002220 ) ) ;
#63077=FACE_OUTER_BOUND ( 'NONE', #65161, .T. ) ;
#63078=DIRECTION ( 'NONE',  ( 0.000000000000000000, 0.9999999999976377785, 2.173523156925979128E-06 ) ) ;
#63079=PLANE ( 'NONE',  #4428 ) ;
#63080=CARTESIAN_POINT ( 'NONE',  ( -8.334044162642690878, 20.12857247364870616, -1.500000000000002220 ) ) ;
#63081=CARTESIAN_POINT ( 'NONE',  ( -67.52287095715003318, -23.47593901973090169, -1.443836447538996870 ) ) ;
#63087=DIRECTION ( 'NONE',  ( 1.000000000000000000, 3.773278334444166432E-23, 8.201307841325785021E-29 ) ) ;
#63089=VERTEX_POINT ( 'NONE', #94406 ) ;
#63090=EDGE_CURVE ( 'NONE', #10228, #41756, #20632, .T. ) ;
#63091=DIRECTION ( 'NONE',  ( 0.000000000000000000, 0.9999999999976377785, 2.173523156925979975E-06 ) ) ;
#63092=CARTESIAN_POINT ( 'NONE',  ( -82.51328383053662208, -23.96119346886881019, -0.6495511937831923710 ) ) ;
#63093=CARTESIAN_POINT ( 'NONE',  ( 7.950249384483326409, 19.69624408967213469, 11.49999999999998934 ) ) ;
#63094=CARTESIAN_POINT ( 'NONE',  ( -94.55207186148825826, -24.15543982623907482, -0.2315651400026595141 ) ) ;
#63095=EDGE_CURVE ( 'NONE', #67184, #32503, #79937, .T. ) ;
#63096=CARTESIAN_POINT ( 'NONE',  ( -69.62287095715005592, -24.66019654487199020, 8.947790411086131712 ) ) ;
#63097=DIRECTION ( 'NONE',  ( -1.000000000000000000, -3.773278334444166432E-23, -8.201307841325785021E-29 ) ) ;
#63099=CARTESIAN_POINT ( 'NONE',  ( 18.72033823704212097, 5.060218808788302880, 11.49999999999998934 ) ) ;
#63101=ORIENTED_EDGE ( 'NONE', *, *, #97357, .T. ) ;
#63102=CARTESIAN_POINT ( 'NONE',  ( -15.27948257512286645, 12.15582775940324822, 11.49999999999999645 ) ) ;
#63103=CARTESIAN_POINT ( 'NONE',  ( -91.52287095715006160, -24.65952944569304606, 1.056160979905700570 ) ) ;
#63106=EDGE_CURVE ( 'NONE', #22592, #5790, #81212, .T. ) ;
#63109=CARTESIAN_POINT ( 'NONE',  ( -89.59823067049254064, -23.73766607897671221, -1.055555164236434029 ) ) ;
#63110=AXIS2_PLACEMENT_3D ( 'NONE', #22842, #30478, #46715 ) ;
#63111=B_SPLINE_CURVE_WITH_KNOTS ( 'NONE', 3,
 ( #39706, #71173, #94501, #93994 ),
 .UNSPECIFIED., .F., .F.,
 ( 4, 4 ),
 ( 0.000000000000000000, 9.999999999997510880E-05 ),
 .UNSPECIFIED. ) ;
#63114=CARTESIAN_POINT ( 'NONE',  ( -17.62174901100306101, -8.731699659924187173, -1.500000000000002220 ) ) ;
#63117=CARTESIAN_POINT ( 'NONE',  ( -20.99440926880444636, 4.982473936180791263, 11.49999999999998934 ) ) ;
#63119=DIRECTION ( 'NONE',  ( -0.000000000000000000, 2.173523156925979552E-06, -0.9999999999976378895 ) ) ;
#63121=CARTESIAN_POINT ( 'NONE',  ( 13.31140876108729998, -18.89465134148960956, -1.500000000000002220 ) ) ;
#63127=CARTESIAN_POINT ( 'NONE',  ( -111.0058427071010527, -25.29823846644867658, 2.995660944314382679 ) ) ;
#63128=CARTESIAN_POINT ( 'NONE',  ( -129.6234738294825206, -24.65952944569305316, 1.056160979905705677 ) ) ;
#63129=CARTESIAN_POINT ( 'NONE',  ( -99.15308351095438866, -25.26400742361759555, 4.278189958765021395 ) ) ;
#63130=CARTESIAN_POINT ( 'NONE',  ( -17.57349146297605103, 9.389787994052484876, -1.500000000000002220 ) ) ;
#63131=CARTESIAN_POINT ( 'NONE',  ( -75.59706082321993392, -24.15602025860895807, 10.28564288303536678 ) ) ;
#63132=CARTESIAN_POINT ( 'NONE',  ( -19.37706247964952411, -4.161318200553020041, -1.500000000000002220 ) ) ;
#63133=ORIENTED_EDGE ( 'NONE', *, *, #29498, .T. ) ;
#63134=CARTESIAN_POINT ( 'NONE',  ( -56.55353067738275286, -23.96119346886880663, -0.6495511937832126881 ) ) ;
#63135=EDGE_CURVE ( 'NONE', #48998, #21576, #71510, .T. ) ;
#63136=CARTESIAN_POINT ( 'NONE',  ( -39.08546997848264226, -25.10925814828167546, 3.855771613512330109 ) ) ;
#63137=DIRECTION ( 'NONE',  ( 0.000000000000000000, 0.9999999999976377785, 2.173523156925979128E-06 ) ) ;
#63138=CARTESIAN_POINT ( 'NONE',  ( 14.61947915221463923, 14.71393552341326760, 11.49999999999999645 ) ) ;
#63139=CARTESIAN_POINT ( 'NONE',  ( -83.62287095715005592, -29.50250243563736774, 8.947779886222141599 ) ) ;
#63140=EDGE_CURVE ( 'NONE', #62812, #82726, #40127, .T. ) ;
#63141=CARTESIAN_POINT ( 'NONE',  ( -38.62287095715005592, -24.64898659630528144, 1.056161002820819261 ) ) ;
#63142=CARTESIAN_POINT ( 'NONE',  ( -4.239441843796335263, -22.36999388947090139, 11.49999999999999645 ) ) ;
#63143=B_SPLINE_CURVE_WITH_KNOTS ( 'NONE', 3,
 ( #51721, #74554, #4558, #35504, #89784, #67450, #81168, #83154, #66962, #42625, #97875, #66480 ),
 .UNSPECIFIED., .F., .F.,
 ( 4, 2, 2, 2, 2, 4 ),
 ( 0.000000000000000000, 0.0003156378818151490723, 0.0006312757636302981446, 0.0009469136454454471627, 0.001104732586353022322, 0.001262551527260597373 ),
 .UNSPECIFIED. ) ;
#63145=PLANE ( 'NONE',  #78634 ) ;
#63146=LINE ( 'NONE', #94071, #72751 ) ;
#63148=CARTESIAN_POINT ( 'NONE',  ( 19.32837167043147986, -5.866312143582237404, -1.500000000000002220 ) ) ;
#63152=CARTESIAN_POINT ( 'NONE',  ( -40.55620429048340014, -23.48786465467240347, 11.44779295918255180 ) ) ;
#63153=CARTESIAN_POINT ( 'NONE',  ( -20.38739128398232836, 10.50225141308550292, 11.49999999999998934 ) ) ;
#63154=CARTESIAN_POINT ( 'NONE',  ( -50.40445135320379677, -25.18439649812517089, 3.293943117865877124 ) ) ;
#63155=CARTESIAN_POINT ( 'NONE',  ( -16.84340083857899018, -10.81494551495373457, -1.500000000000002220 ) ) ;
#63156=CARTESIAN_POINT ( 'NONE',  ( -71.52287095715010423, -24.66019654487200086, 8.947790411086115725 ) ) ;
#63157=CARTESIAN_POINT ( 'NONE',  ( 20.71091302404612833, 3.140364381853995912, 11.49999999999999645 ) ) ;
#63159=CARTESIAN_POINT ( 'NONE',  ( -68.96115101070704156, -25.31612651568953254, 5.914983513647228186 ) ) ;
#63160=CARTESIAN_POINT ( 'NONE',  ( -21.92701646642465008, -2.088449908657787457, -1.500000000000002220 ) ) ;
#63164=CARTESIAN_POINT ( 'NONE',  ( -127.4728709548940486, -25.21112548385454843, 2.000950964958115197 ) ) ;
#63165=VERTEX_POINT ( 'NONE', #36004 ) ;
#63166=CARTESIAN_POINT ( 'NONE',  ( -49.54012794836013001, -25.27344868860170379, 3.796733121357704022 ) ) ;
#63168=ORIENTED_EDGE ( 'NONE', *, *, #84588, .F. ) ;
#63169=FACE_OUTER_BOUND ( 'NONE', #34714, .T. ) ;
#63170=ORIENTED_EDGE ( 'NONE', *, *, #40223, .T. ) ;
#63173=CARTESIAN_POINT ( 'NONE',  ( -100.6747599127204040, -25.10935806245408841, 2.849795651036889588 ) ) ;
#63174=CARTESIAN_POINT ( 'NONE',  ( -36.58086577407884477, -24.51314013834316086, 0.6176544820404111791 ) ) ;
#63175=CARTESIAN_POINT ( 'NONE',  ( -9.379331868514380943, 18.20734191464070406, -1.500000000000002220 ) ) ;
#63178=ADVANCED_FACE ( 'NONE', ( #97891 ), #28387, .F. ) ;
#63179=AXIS2_PLACEMENT_3D ( 'NONE', #16888, #38223, #47849 ) ;
#63180=CARTESIAN_POINT ( 'NONE',  ( -44.54662673226112446, -24.15543982623906771, -0.2315651400026670914 ) ) ;
#63181=CARTESIAN_POINT ( 'NONE',  ( -54.62287095715004881, -23.48783264082478084, -1.443836473390070596 ) ) ;
#63182=CARTESIAN_POINT ( 'NONE',  ( -21.75032768068154354, -4.810781854073628239, 11.49999999999998934 ) ) ;
#63183=CARTESIAN_POINT ( 'NONE',  ( -101.5895376238167245, -24.64965694238407679, 8.947790433994649462 ) ) ;
#63184=CARTESIAN_POINT ( 'NONE',  ( -81.52287095715006160, -29.50248528299804818, 1.056150453629038477 ) ) ;
#63186=B_SPLINE_CURVE_WITH_KNOTS ( 'NONE', 3,
 ( #84791, #28511, #67592, #15275 ),
 .UNSPECIFIED., .F., .F.,
 ( 4, 4 ),
 ( 0.000000000000000000, 0.0001002978966067895783 ),
 .UNSPECIFIED. ) ;
#63187=DIRECTION ( 'NONE',  ( -3.773278334453079618E-23, 0.9999999999976377785, 2.173523156925979975E-06 ) ) ;
#63189=DIRECTION ( 'NONE',  ( 0.000000000000000000, 2.173523156925980399E-06, -0.9999999999976378895 ) ) ;
#63191=CARTESIAN_POINT ( 'NONE',  ( -19.40898059523135544, 7.551958013340856368, 11.49999999999998934 ) ) ;
#63192=ORIENTED_EDGE ( 'NONE', *, *, #21717, .F. ) ;
#63194=ORIENTED_EDGE ( 'NONE', *, *, #52191, .T. ) ;
#63195=VERTEX_POINT ( 'NONE', #12663 ) ;
#63196=AXIS2_PLACEMENT_3D ( 'NONE', #62854, #31882, #24263 ) ;
#63197=CARTESIAN_POINT ( 'NONE',  ( -51.52589570729855950, -25.12217672741640584, 6.227984225844234167 ) ) ;
#63198=CARTESIAN_POINT ( 'NONE',  ( -16.09219062524700661, 13.46031615953476468, -1.500000000000002220 ) ) ;
#63199=ORIENTED_EDGE ( 'NONE', *, *, #71911, .T. ) ;
#63200=CARTESIAN_POINT ( 'NONE',  ( -93.62287095715002749, -24.51387760970724727, 9.387446482453412955 ) ) ;
#63203=CARTESIAN_POINT ( 'NONE',  ( -86.59885718012090194, -23.73791477778911840, 11.05961554403170766 ) ) ;
#63204=CARTESIAN_POINT ( 'NONE',  ( -60.62287095715006302, -24.91570333823099404, 8.075032458375554612 ) ) ;
#63206=EDGE_CURVE ( 'NONE', #14471, #47759, #49781, .T. ) ;
#63207=CARTESIAN_POINT ( 'NONE',  ( 19.86420646539740176, -9.926203236129387264, 11.49999999999999645 ) ) ;
#63209=CARTESIAN_POINT ( 'NONE',  ( -109.2228709571500644, -23.47593901973090524, -1.443836447538996648 ) ) ;
#63210=CARTESIAN_POINT ( 'NONE',  ( -37.58953762381672448, -23.48786465467240347, 11.44779295918255180 ) ) ;
#63212=CARTESIAN_POINT ( 'NONE',  ( -14.80616194778269623, -17.16973004002414882, -1.500000000000002220 ) ) ;
#63214=EDGE_LOOP ( 'NONE', ( #86301, #94875, #15980, #43963 ) ) ;
#63215=EDGE_LOOP ( 'NONE', ( #42970, #31099, #51835, #64970 ) ) ;
#63218=CARTESIAN_POINT ( 'NONE',  ( 2.654622155064554789, -19.98241913370796041, 11.49999999999998934 ) ) ;
#63220=CARTESIAN_POINT ( 'NONE',  ( -81.62287095715004170, -24.51387760970723662, 9.387446482453421837 ) ) ;
#63221=ORIENTED_EDGE ( 'NONE', *, *, #36699, .T. ) ;
#63222=CARTESIAN_POINT ( 'NONE',  ( -39.52287095715006870, -23.48786465467241058, 11.44779295918255180 ) ) ;
#63223=CARTESIAN_POINT ( 'NONE',  ( -17.59303920844588376, -13.82112144285918731, -1.500000000000002220 ) ) ;
#63224=EDGE_CURVE ( 'NONE', #19118, #74917, #98390, .T. ) ;
#63228=CARTESIAN_POINT ( 'NONE',  ( -94.55206473217479868, -24.15620529776628089, 10.23563542870660470 ) ) ;
#63229=CARTESIAN_POINT ( 'NONE',  ( -96.55620429048340725, -23.47596703998600631, 11.44779298504227683 ) ) ;
#63233=CARTESIAN_POINT ( 'NONE',  ( 6.425176733589397671, 18.50107501292125178, -1.500000000000002220 ) ) ;
#63235=ORIENTED_EDGE ( 'NONE', *, *, #1321, .T. ) ;
#63236=CARTESIAN_POINT ( 'NONE',  ( 2.564635614221720594, -21.35862533600356983, -1.500000000000002220 ) ) ;
#63237=CARTESIAN_POINT ( 'NONE',  ( -102.5228709571500758, -23.48786465467241769, 11.44779295918254114 ) ) ;
#63239=CARTESIAN_POINT ( 'NONE',  ( -71.62287095715005592, -23.48786465467241413, 11.44779295918254469 ) ) ;
#63241=CARTESIAN_POINT ( 'NONE',  ( -68.62287095715007013, -23.72773821059536559, 11.05748984161097681 ) ) ;
#63242=CARTESIAN_POINT ( 'NONE',  ( 22.74528686061176685, 3.085755641335488964, -1.500000000000002220 ) ) ;
#63245=DIRECTION ( 'NONE',  ( -3.773278334453079618E-23, 0.9999999999976377785, 2.173523156925978705E-06 ) ) ;
#63246=CARTESIAN_POINT ( 'NONE',  ( -14.99618758923778117, -13.25627519679515665, 11.49999999999999645 ) ) ;
#63248=CARTESIAN_POINT ( 'NONE',  ( -46.52287095715006160, -29.50248528299804818, 1.056150453629033370 ) ) ;
#63249=VECTOR ( 'NONE', #21338, 1000.000000000000114 ) ;
#63251=CARTESIAN_POINT ( 'NONE',  ( -60.52287095715006160, -23.48786465467241058, 11.44779295918254824 ) ) ;
#63252=ORIENTED_EDGE ( 'NONE', *, *, #10579, .T. ) ;
#63255=CARTESIAN_POINT ( 'NONE',  ( 19.96715809174937561, -8.635335823514383335, 11.49999999999998934 ) ) ;
#63257=CARTESIAN_POINT ( 'NONE',  ( 5.252985061998082017, 18.97096265210048571, -1.500000000000002220 ) ) ;
#63258=CARTESIAN_POINT ( 'NONE',  ( -27.70544111104076990, -24.60484793945295934, 1.628749883096155981 ) ) ;
#63259=EDGE_CURVE ( 'NONE', #84371, #53585, #73828, .T. ) ;
#63261=CARTESIAN_POINT ( 'NONE',  ( -109.3640311185025098, -25.31697976619958013, 4.352105570880266505 ) ) ;
#63263=VECTOR ( 'NONE', #96849, 1000.000000000000114 ) ;
#63264=FACE_OUTER_BOUND ( 'NONE', #31560, .T. ) ;
#63266=CARTESIAN_POINT ( 'NONE',  ( -15.41819309731374510, 13.62919173607049927, 11.49999999999999645 ) ) ;
#63268=B_SPLINE_CURVE_WITH_KNOTS ( 'NONE', 3,
 ( #7278, #99617, #92020, #85913 ),
 .UNSPECIFIED., .F., .F.,
 ( 4, 4 ),
 ( 0.000000000000000000, 9.999999999998897304E-05 ),
 .UNSPECIFIED. ) ;
#63269=CARTESIAN_POINT ( 'NONE',  ( -47.62287095715007723, -24.34917612406837861, 0.1852690917426594308 ) ) ;
#63271=CARTESIAN_POINT ( 'NONE',  ( -20.05226876979747530, -10.47825485868949613, 11.49999999999999645 ) ) ;
#63272=EDGE_CURVE ( 'NONE', #15143, #72803, #21869, .T. ) ;
#63273=ORIENTED_EDGE ( 'NONE', *, *, #96308, .F. ) ;
#63275=CARTESIAN_POINT ( 'NONE',  ( -99.59758909298055585, -25.26387354126681117, 4.277504120023178480 ) ) ;
#63278=CARTESIAN_POINT ( 'NONE',  ( -74.52287095715007581, -23.47596703998600631, 11.44779298504228748 ) ) ;
#63280=CARTESIAN_POINT ( 'NONE',  ( -25.53098197642538736, -24.93062915712978977, 4.942811675010964301 ) ) ;
#63283=CARTESIAN_POINT ( 'NONE',  ( -79.71799800425125682, -25.31596267615770657, 5.176233665374946114 ) ) ;
#63284=CARTESIAN_POINT ( 'NONE',  ( 2.723195454624489642, 22.67993996152103620, -1.500000000000002220 ) ) ;
#63285=DIRECTION ( 'NONE',  ( 0.000000000000000000, -0.9999999999976377785, -2.173523156925979552E-06 ) ) ;
#63287=CARTESIAN_POINT ( 'NONE',  ( -63.63676845969973073, -24.15620529776628089, 10.23563542870660470 ) ) ;
#63288=CARTESIAN_POINT ( 'NONE',  ( -18.83616483605274539, -12.25834331966736102, 11.49999999999999645 ) ) ;
#63290=CARTESIAN_POINT ( 'NONE',  ( -86.52287095715006160, -29.50248528299804818, 1.056150453629040253 ) ) ;
#63291=CARTESIAN_POINT ( 'NONE',  ( -4.809782828112996178, 21.40371668077904488, -1.500000000000002220 ) ) ;
#63292=CARTESIAN_POINT ( 'NONE',  ( -126.8949105597723417, -25.34741607406076724, 3.801658267186113438 ) ) ;
#63293=EDGE_CURVE ( 'NONE', #41031, #36561, #59860, .T. ) ;
#63294=CARTESIAN_POINT ( 'NONE',  ( -44.59357593954516119, -24.15620529776627734, 10.23563542870660470 ) ) ;
#63295=CARTESIAN_POINT ( 'NONE',  ( -69.21694530810552237, -25.13479670434804447, 7.034542371138676309 ) ) ;
#63299=VERTEX_POINT ( 'NONE', #75549 ) ;
#63300=CARTESIAN_POINT ( 'NONE',  ( -7.951223608505463503, 18.87544906973805325, 11.49999999999998934 ) ) ;
#63305=B_SPLINE_CURVE_WITH_KNOTS ( 'NONE', 3,
 ( #34242, #81906, #58575, #12384 ),
 .UNSPECIFIED., .F., .F.,
 ( 4, 4 ),
 ( 0.06880487856767243671, 0.06980562560843792119 ),
 .UNSPECIFIED. ) ;
#63306=CARTESIAN_POINT ( 'NONE',  ( -17.14199295335891904, -15.44578658782692671, 11.49999999999998934 ) ) ;
#63307=CARTESIAN_POINT ( 'NONE',  ( -112.5228709571500616, -23.96177878511310055, 10.65340807706329507 ) ) ;
#63308=CARTESIAN_POINT ( 'NONE',  ( -3.898967980886277829, 19.90457959416237088, -1.500000000000002220 ) ) ;
#63309=ORIENTED_EDGE ( 'NONE', *, *, #38589, .F. ) ;
#63310=EDGE_CURVE ( 'NONE', #66922, #94858, #6076, .T. ) ;
#63313=CARTESIAN_POINT ( 'NONE',  ( -92.54656292449074328, -24.51314013834316796, 0.6176544820404240577 ) ) ;
#63317=CARTESIAN_POINT ( 'NONE',  ( 10.13398631766115443, 18.95262098133242290, 11.49999999999999645 ) ) ;
#63318=ORIENTED_EDGE ( 'NONE', *, *, #48249, .F. ) ;
#63319=CARTESIAN_POINT ( 'NONE',  ( -75.55895860488308813, -23.85016227208580730, -0.8807180028928284221 ) ) ;
#63320=CARTESIAN_POINT ( 'NONE',  ( -104.6228709571500985, -24.50216790748100237, 0.6166512839513698108 ) ) ;
#63322=ORIENTED_EDGE ( 'NONE', *, *, #46793, .F. ) ;
#63323=CARTESIAN_POINT ( 'NONE',  ( 15.70846742882596025, 13.54617332914617478, -1.500000000000002220 ) ) ;
#63326=DIRECTION ( 'NONE',  ( -3.773278334453079030E-23, 0.9999999999976377785, 2.173523156925979128E-06 ) ) ;
#63327=ORIENTED_EDGE ( 'NONE', *, *, #18637, .T. ) ;
#63328=CARTESIAN_POINT ( 'NONE',  ( -41.64787139066377364, -23.96169478059712432, 10.65365249895718591 ) ) ;
#63329=CARTESIAN_POINT ( 'NONE',  ( -76.62287095715007013, -29.50247984919015209, -1.443849546365053582 ) ) ;
#63331=VERTEX_POINT ( 'NONE', #61360 ) ;
#63332=CARTESIAN_POINT ( 'NONE',  ( -28.62287095715004526, -24.50732993938405357, 8.947790418389013567 ) ) ;
#63333=CARTESIAN_POINT ( 'NONE',  ( -116.9228709571500389, -23.47596703998600276, 11.44779298504227860 ) ) ;
#63334=CARTESIAN_POINT ( 'NONE',  ( -52.62287095715005592, -29.50250786944525672, 11.44777988621624054 ) ) ;
#63335=EDGE_CURVE ( 'NONE', #25620, #14844, #38774, .T. ) ;
#63336=EDGE_CURVE ( 'NONE', #53781, #26222, #83526, .T. ) ;
#63337=CARTESIAN_POINT ( 'NONE',  ( 20.22059317821533853, 8.664326447042464352, 11.49999999999999645 ) ) ;
#63339=CARTESIAN_POINT ( 'NONE',  ( -20.69567741759225399, -9.018594580484563750, 11.49999999999998934 ) ) ;
#63340=CARTESIAN_POINT ( 'NONE',  ( 16.30764028314251846, 13.22082560946828522, -1.500000000000002220 ) ) ;
#63343=AXIS2_PLACEMENT_3D ( 'NONE', #55610, #54111, #54599 ) ;
#63344=ORIENTED_EDGE ( 'NONE', *, *, #34820, .T. ) ;
#63347=ADVANCED_FACE ( 'NONE', ( #14662 ), #27161, .T. ) ;
#63349=ORIENTED_EDGE ( 'NONE', *, *, #44619, .F. ) ;
#63350=CARTESIAN_POINT ( 'NONE',  ( 17.87031378931267867, -11.31994873005049129, 11.49999999999998934 ) ) ;
#63352=B_SPLINE_CURVE_WITH_KNOTS ( 'NONE', 3,
 ( #62749, #93666, #38385, #16040 ),
 .UNSPECIFIED., .F., .F.,
 ( 4, 4 ),
 ( 0.000000000000000000, 1.000000000000000000 ),
 .UNSPECIFIED. ) ;
#63353=CARTESIAN_POINT ( 'NONE',  ( -50.40895856474225667, -25.03148742036013630, 7.563174219458152159 ) ) ;
#63354=CARTESIAN_POINT ( 'NONE',  ( -121.6234957139205193, -24.65952944569305316, 1.056160979905707897 ) ) ;
#63355=CARTESIAN_POINT ( 'NONE',  ( -120.5228709571500616, -24.99156044556120904, 7.747789690856173195 ) ) ;
#63357=CARTESIAN_POINT ( 'NONE',  ( 20.70802603420765564, 8.137917507125113303, -1.500000000000002220 ) ) ;
#63358=CARTESIAN_POINT ( 'NONE',  ( -114.5542499131790777, -24.15543982623907837, -0.2315651400026444429 ) ) ;
#63360=B_SPLINE_CURVE_WITH_KNOTS ( 'NONE', 3,
 ( #1077, #22878, #15786, #53368, #23899, #53866 ),
 .UNSPECIFIED., .F., .F.,
 ( 4, 2, 4 ),
 ( 1.571603873469763250E-05, 0.001396933878470195617, 0.002778151718205693673 ),
 .UNSPECIFIED. ) ;
#63364=CARTESIAN_POINT ( 'NONE',  ( -126.6245542812432774, -23.96119346886880663, -0.6495511937832031402 ) ) ;
#63368=ADVANCED_FACE ( 'NONE', ( #1958 ), #55250, .F. ) ;
#63369=CARTESIAN_POINT ( 'NONE',  ( 16.53150372360616771, 10.32350692489952593, -1.500000000000002220 ) ) ;
#63370=CARTESIAN_POINT ( 'NONE',  ( 13.27131465344908001, -16.79725507166503462, 11.49999999999998934 ) ) ;
#63372=CARTESIAN_POINT ( 'NONE',  ( -60.63669123105633219, -24.52399227489755518, 9.353111116819372128 ) ) ;
#63373=PLANE ( 'NONE',  #30870 ) ;
#63375=CARTESIAN_POINT ( 'NONE',  ( -4.239441843796335263, -22.36999388947090139, -1.500000000000002220 ) ) ;
#63377=CARTESIAN_POINT ( 'NONE',  ( -98.52218359600611564, -23.48783264082476663, -1.443836473390090136 ) ) ;
#63378=DIRECTION ( 'NONE',  ( -3.773278334444167608E-23, 1.000000000000000000, 0.000000000000000000 ) ) ;
#63379=CARTESIAN_POINT ( 'NONE',  ( -13.97081141688431138, 14.13901428111770819, 11.49999999999999645 ) ) ;
#63380=CARTESIAN_POINT ( 'NONE',  ( -84.52287095715007581, -23.48783264082477018, -1.443836473390090802 ) ) ;
#63381=CARTESIAN_POINT ( 'NONE',  ( -89.81226385320383088, -25.05712135967894838, 7.447789548357302891 ) ) ;
#63384=LINE ( 'NONE', #17682, #21783 ) ;
#63385=CARTESIAN_POINT ( 'NONE',  ( -50.62287095715005592, -29.50247984919015209, -1.443849546365058689 ) ) ;
#63387=CARTESIAN_POINT ( 'NONE',  ( 2.186256072416925544, -21.55203199515037582, 11.49999999999998934 ) ) ;
#63389=CARTESIAN_POINT ( 'NONE',  ( -19.46337940159461866, -0.4807646128305608779, -1.500000000000002220 ) ) ;
#63390=CARTESIAN_POINT ( 'NONE',  ( -123.6228709571500559, -23.48786465467241769, 11.44779295918253759 ) ) ;
#63392=CARTESIAN_POINT ( 'NONE',  ( 19.51578053514377586, 5.923290232019536639, 11.49999999999999645 ) ) ;
#63393=DIRECTION ( 'NONE',  ( 1.000000000000000000, 3.773278334444167608E-23, 8.201307833595939069E-29 ) ) ;
#63395=FACE_OUTER_BOUND ( 'NONE', #70018, .T. ) ;
#63397=CARTESIAN_POINT ( 'NONE',  ( -79.12743195124619433, -25.17601835801890076, 6.783621481769894324 ) ) ;
#63398=CARTESIAN_POINT ( 'NONE',  ( -29.62287095715003105, -23.66062849325336259, -1.053491143263840746 ) ) ;
#63400=CARTESIAN_POINT ( 'NONE',  ( -125.6228709571500559, -23.48786465467241769, 11.44779295918253403 ) ) ;
#63402=CARTESIAN_POINT ( 'NONE',  ( 14.11618873683251252, 14.29484301466228047, -1.500000000000002220 ) ) ;
#63404=ORIENTED_EDGE ( 'NONE', *, *, #15552, .F. ) ;
#63408=CARTESIAN_POINT ( 'NONE',  ( -15.63304604236160067, -16.83380969201049382, 11.49999999999999645 ) ) ;
#63409=CARTESIAN_POINT ( 'NONE',  ( 16.28376985728763415, 15.88423345705086298, -1.500000000000002220 ) ) ;
#63411=CARTESIAN_POINT ( 'NONE',  ( -31.52287095715006160, -23.47596703998600631, 11.44779298504229459 ) ) ;
#63412=CARTESIAN_POINT ( 'NONE',  ( -75.62287095715009855, -24.83620972994592435, 8.398175272781363887 ) ) ;
#63413=CARTESIAN_POINT ( 'NONE',  ( -81.52287095715007581, -24.33927499327856125, 9.819080762295815390 ) ) ;
#63414=CARTESIAN_POINT ( 'NONE',  ( -61.47555918000787756, -25.07008561068857588, 7.435194656350822662 ) ) ;
#63418=CARTESIAN_POINT ( 'NONE',  ( -76.62287095715007013, -24.66019654487199730, 8.947790411086128159 ) ) ;
#63419=CARTESIAN_POINT ( 'NONE',  ( -58.52207422368198309, -23.48783264082477018, -1.443836473390093689 ) ) ;
#63420=VERTEX_POINT ( 'NONE', #55751 ) ;
#63422=CARTESIAN_POINT ( 'NONE',  ( -18.82316870354832616, 7.800066519331792847, 11.49999999999998934 ) ) ;
#63425=CARTESIAN_POINT ( 'NONE',  ( -12.88233675513024856, -19.01995677650982230, 11.49999999999998934 ) ) ;
#63427=EDGE_CURVE ( 'NONE', #54139, #100298, #19371, .T. ) ;
#63428=ORIENTED_EDGE ( 'NONE', *, *, #84339, .F. ) ;
#63429=CARTESIAN_POINT ( 'NONE',  ( -101.6228709571500559, -24.65952944569304606, 1.056160979905702790 ) ) ;
#63433=CARTESIAN_POINT ( 'NONE',  ( -117.2171617987493448, -25.23514715042687229, 6.311476322788518445 ) ) ;
#63434=CARTESIAN_POINT ( 'NONE',  ( -13.37813101364405100, 16.61575060780308277, 11.49999999999999645 ) ) ;
#63437=CARTESIAN_POINT ( 'NONE',  ( -8.951960448472247478, 20.35530821588910300, 11.49999999999998934 ) ) ;
#63438=CARTESIAN_POINT ( 'NONE',  ( 17.27521350410721368, -11.31798593588896829, -1.500000000000002220 ) ) ;
#63440=VERTEX_POINT ( 'NONE', #80068 ) ;
#63442=CARTESIAN_POINT ( 'NONE',  ( -95.58393028260560698, -24.92592662359561473, 8.075495903017998245 ) ) ;
#63443=ORIENTED_EDGE ( 'NONE', *, *, #93919, .T. ) ;
#63444=CARTESIAN_POINT ( 'NONE',  ( -87.62287095715004170, -24.64898659630528854, 1.056161002820827921 ) ) ;
#63446=CARTESIAN_POINT ( 'NONE',  ( -58.64320803498131340, -23.96169478059713143, 10.65365249895718058 ) ) ;
#63448=CARTESIAN_POINT ( 'NONE',  ( 18.69404101259207707, 9.334567778723176446, -1.500000000000002220 ) ) ;
#63450=CARTESIAN_POINT ( 'NONE',  ( -4.983756199382824548, -21.29032736245130053, 11.49999999999999645 ) ) ;
#63453=CARTESIAN_POINT ( 'NONE',  ( 14.28312119630281174, -17.39864199977734671, -1.500000000000002220 ) ) ;
#63454=CARTESIAN_POINT ( 'NONE',  ( -118.5181897846719181, -24.35071581493543746, 9.817618358456021710 ) ) ;
#63455=CARTESIAN_POINT ( 'NONE',  ( -72.52287095715010423, -24.51387760970725083, 9.387446482453427166 ) ) ;
#63459=ORIENTED_EDGE ( 'NONE', *, *, #82458, .F. ) ;
#63460=ORIENTED_EDGE ( 'NONE', *, *, #76059, .F. ) ;
#63462=CARTESIAN_POINT ( 'NONE',  ( -99.41830603981939873, -25.12215564308212024, 6.591151844143220195 ) ) ;
#63463=VERTEX_POINT ( 'NONE', #18168 ) ;
#63464=CARTESIAN_POINT ( 'NONE',  ( -21.42254595866439004, -0.3319015934494286557, -1.500000000000002220 ) ) ;
#63465=CARTESIAN_POINT ( 'NONE',  ( 17.53502452033532677, 13.85421504792973479, 11.49999999999999645 ) ) ;
#63468=CARTESIAN_POINT ( 'NONE',  ( -17.44821286160079410, -11.81026508430653088, -1.500000000000002220 ) ) ;
#63469=CARTESIAN_POINT ( 'NONE',  ( -30.49971861685504138, -24.27034544923275661, 9.960304333224314632 ) ) ;
#63470=CARTESIAN_POINT ( 'NONE',  ( 13.89251353435424363, -14.32104260081073832, -1.500000000000002220 ) ) ;
#63471=DIRECTION ( 'NONE',  ( -3.773278334453079030E-23, 0.9999999999976377785, 2.173523156925979128E-06 ) ) ;
#63473=CARTESIAN_POINT ( 'NONE',  ( -1.213202359833694732, 22.00568734548514627, -1.500000000000002220 ) ) ;
#63474=CARTESIAN_POINT ( 'NONE',  ( -52.62287095715005592, -23.47593901973091235, -1.443836447539009749 ) ) ;
#63476=CARTESIAN_POINT ( 'NONE',  ( -65.58909869047282371, -24.52399227489126687, 9.353111116836526406 ) ) ;
#63477=B_SPLINE_CURVE_WITH_KNOTS ( 'NONE', 3,
 ( #95513, #55461, #55968, #86398 ),
 .UNSPECIFIED., .F., .F.,
 ( 4, 4 ),
 ( 0.000000000000000000, 9.999999999998897304E-05 ),
 .UNSPECIFIED. ) ;
#63479=CARTESIAN_POINT ( 'NONE',  ( -14.93763623016880082, -14.57113377498261997, 11.49999999999999645 ) ) ;
#63480=EDGE_CURVE ( 'NONE', #24375, #33030, #50835, .T. ) ;
#63484=CARTESIAN_POINT ( 'NONE',  ( -61.55620429048339304, -24.65952944569304606, 1.056160979905697461 ) ) ;
#63485=CARTESIAN_POINT ( 'NONE',  ( -3.453506354162970915, -21.03206338698385736, -1.500000000000002220 ) ) ;
#63486=CARTESIAN_POINT ( 'NONE',  ( -71.62287095715005592, -23.47596703998600631, 11.44779298504227683 ) ) ;
#63487=CARTESIAN_POINT ( 'NONE',  ( -50.91374622504534386, -25.21061005848796555, 3.406474964634027103 ) ) ;
#63488=EDGE_CURVE ( 'NONE', #60161, #82250, #8602, .T. ) ;
#63489=CARTESIAN_POINT ( 'NONE',  ( -71.55620429048339304, -24.65952944569304606, 1.056160979905697461 ) ) ;
#63491=CARTESIAN_POINT ( 'NONE',  ( 22.48772827135616126, 0.8316936486096353498, -1.500000000000002220 ) ) ;
#63494=CARTESIAN_POINT ( 'NONE',  ( -79.10665409224128553, -25.30355450193266975, 5.239253019725047089 ) ) ;
#63496=CARTESIAN_POINT ( 'NONE',  ( 19.18734209777730015, 4.435579877058994036, 11.49999999999999645 ) ) ;
#63497=CARTESIAN_POINT ( 'NONE',  ( -32.07722060962682775, -25.12026506542016335, 2.831122744435439209 ) ) ;
#63498=CARTESIAN_POINT ( 'NONE',  ( -39.52287095715006870, -24.64898659630528144, 1.056161002820819261 ) ) ;
#63499=B_SPLINE_CURVE_WITH_KNOTS ( 'NONE', 3,
 ( #29576, #60553, #61041, #75251 ),
 .UNSPECIFIED., .F., .F.,
 ( 4, 4 ),
 ( 0.4708362126144793325, 0.4798426438865949217 ),
 .UNSPECIFIED. ) ;
#63502=LINE ( 'NONE', #78184, #67537 ) ;
#63503=CARTESIAN_POINT ( 'NONE',  ( -124.5553377431336486, -24.15620529776629510, 10.23563542870659404 ) ) ;
#63504=B_SPLINE_CURVE_WITH_KNOTS ( 'NONE', 3,
 ( #35214, #27604, #13351, #58553 ),
 .UNSPECIFIED., .F., .F.,
 ( 4, 4 ),
 ( 0.05053608658242522006, 0.05954251785454105911 ),
 .UNSPECIFIED. ) ;
#63506=CARTESIAN_POINT ( 'NONE',  ( -8.281543130087330340, -17.94227898472161797, 11.49999999999998934 ) ) ;
#63508=CARTESIAN_POINT ( 'NONE',  ( 0.4983251850863967269, 20.17815531296474418, 11.49999999999999645 ) ) ;
#63514=CARTESIAN_POINT ( 'NONE',  ( -82.92287095715010992, -23.47593901973090524, -1.443836447538997536 ) ) ;
#63515=DIRECTION ( 'NONE',  ( -3.773278334453079030E-23, 0.9999999999976377785, 2.173523156925979128E-06 ) ) ;
#63516=CARTESIAN_POINT ( 'NONE',  ( -61.52287095715007581, -23.48783264082476308, -1.443836473390092356 ) ) ;
#63517=CARTESIAN_POINT ( 'NONE',  ( 10.17626895549074817, -17.22257424524772418, 11.49999999999998934 ) ) ;
#63518=DIRECTION ( 'NONE',  ( -3.773278334453079030E-23, 0.9999999999976377785, 2.173523156925979128E-06 ) ) ;
#63519=CARTESIAN_POINT ( 'NONE',  ( -116.6262418075701817, -24.15620529776629155, 10.23563542870659759 ) ) ;
#63520=ORIENTED_EDGE ( 'NONE', *, *, #99905, .T. ) ;
#63521=CARTESIAN_POINT ( 'NONE',  ( -104.6228709571500559, -24.51387760970723306, 9.387446482453396968 ) ) ;
#63522=LINE ( 'NONE', #92936, #34612 ) ;
#63523=CARTESIAN_POINT ( 'NONE',  ( -118.5228709571500758, -23.48786465467241769, 11.44779295918253759 ) ) ;
#63525=VECTOR ( 'NONE', #45657, 1000.000000000000114 ) ;
#63526=CARTESIAN_POINT ( 'NONE',  ( -124.5562042904833930, -24.65952944569305316, 1.056160979905708119 ) ) ;
#63527=CARTESIAN_POINT ( 'NONE',  ( -83.50336294561820694, -24.51314013834315375, 0.6176544820404104019 ) ) ;
#63530=FACE_OUTER_BOUND ( 'NONE', #33042, .T. ) ;
#63532=EDGE_CURVE ( 'NONE', #93020, #47315, #68975, .T. ) ;
#63533=B_SPLINE_CURVE_WITH_KNOTS ( 'NONE', 3,
 ( #37128, #27153, #21881, #52859, #45250, #76175 ),
 .UNSPECIFIED., .F., .F.,
 ( 4, 2, 4 ),
 ( 6.391158118964603462E-06, 0.001387004593080780942, 0.002767618028042597225 ),
 .UNSPECIFIED. ) ;
#63534=CARTESIAN_POINT ( 'NONE',  ( 6.837353022973060135, 19.10023500134885310, 11.49999999999998934 ) ) ;
#63535=B_SPLINE_CURVE_WITH_KNOTS ( 'NONE', 3,
 ( #34268, #73329, #41377, #26651, #26142, #88052, #89052, #88551, #80432, #25642, #87546, #79421, #10923, #40869, #96162, #95158, #41887, #57115, #71829, #42883, #96651, #65241, #95661, #48995, #2322, #19026, #48497, #87039, #33761, #18527, #72834, #27149, #73815, #56617, #10415, #50001, #33251, #80934, #3822, #25131, #11421, #58115, #64744, #42396, #64233, #19523, #72329, #50487, #11918, #32752, #18028, #79924, #12907, #60111 ),
 .UNSPECIFIED., .F., .F.,
 ( 4, 1, 1, 1, 1, 2, 2, 1, 2, 2, 1, 1, 2, 2, 1, 2, 2, 2, 1, 2, 2, 1, 1, 1, 2, 2, 1, 2, 2, 1, 1, 1, 2, 2, 4 ),
 ( 0.000000000000000000, 0.06250000000000152656, 0.09375000000000245637, 0.1093750000000030947, 0.1171875000000032474, 0.1210937500000031780, 0.1250000000000031086, 0.1562500000000031364, 0.1718750000000030254, 0.1875000000000029143, 0.2187500000000029421, 0.2343750000000028311, 0.2421875000000027478, 0.2500000000000026645, 0.3125000000000017764, 0.3437500000000013323, 0.3750000000000008882, 0.4999999999999987232, 0.5624999999999977796, 0.5937499999999972244, 0.6249999999999965583, 0.6874999999999955591, 0.7187499999999950040, 0.7343749999999950040, 0.7421874999999950040, 0.7499999999999951150, 0.7812499999999951150, 0.7968749999999953371, 0.8124999999999956701, 0.8437499999999961142, 0.8593749999999962252, 0.8671874999999961142, 0.8710937499999964473, 0.8749999999999966693, 1.000000000000000000 ),
 .UNSPECIFIED. ) ;
#63538=CARTESIAN_POINT ( 'NONE',  ( -34.59403392823487167, -24.15543982623907127, -0.2315651400026574880 ) ) ;
#63540=PLANE ( 'NONE',  #65483 ) ;
#63542=ORIENTED_EDGE ( 'NONE', *, *, #44876, .F. ) ;
#63543=CARTESIAN_POINT ( 'NONE',  ( -81.62287095715004170, -23.96127896941632685, -0.6493128931037849272 ) ) ;
#63544=VECTOR ( 'NONE', #6923, 1000.000000000000114 ) ;
#63545=CARTESIAN_POINT ( 'NONE',  ( 19.32837167043147986, -5.866312143582237404, -1.500000000000002220 ) ) ;
#63547=CARTESIAN_POINT ( 'NONE',  ( -19.39432879369159224, 8.380699159679657839, 11.49999999999999645 ) ) ;
#63549=CARTESIAN_POINT ( 'NONE',  ( -10.67647856527443473, 19.39090429279614369, -1.500000000000002220 ) ) ;
#63551=CARTESIAN_POINT ( 'NONE',  ( 16.43461662053371697, -12.34185696772103391, 11.49999999999998934 ) ) ;
#63552=CARTESIAN_POINT ( 'NONE',  ( -79.52287095715006160, -23.47596703998600631, 11.44779298504228571 ) ) ;
#63553=VERTEX_POINT ( 'NONE', #99703 ) ;
#63554=CARTESIAN_POINT ( 'NONE',  ( -94.62287095715005592, -24.66019654487199730, 8.947790411086126383 ) ) ;
#63555=VERTEX_POINT ( 'NONE', #63181 ) ;
#63557=CARTESIAN_POINT ( 'NONE',  ( -104.6228709571500559, -24.65952944569304961, 1.056160979905701236 ) ) ;
#63559=ORIENTED_EDGE ( 'NONE', *, *, #35178, .T. ) ;
#63560=EDGE_LOOP ( 'NONE', ( #17608, #14709, #6777, #2894, #5894 ) ) ;
#63561=CARTESIAN_POINT ( 'NONE',  ( -111.6379088208709760, -25.24256088085423499, 3.668351635140509881 ) ) ;
#63562=PLANE ( 'NONE',  #40564 ) ;
#63564=CARTESIAN_POINT ( 'NONE',  ( -17.53982812869053731, -11.02811673548155902, -1.500000000000002220 ) ) ;
#63565=CARTESIAN_POINT ( 'NONE',  ( 10.55456386191721663, 18.89434267519128596, 11.49999999999999645 ) ) ;
#63568=CARTESIAN_POINT ( 'NONE',  ( -109.6228709571500417, -23.48786465467242124, 11.44779295918253936 ) ) ;
#63569=CARTESIAN_POINT ( 'NONE',  ( 17.95543856985664277, -13.40637504462900331, -1.500000000000002220 ) ) ;
#63570=CARTESIAN_POINT ( 'NONE',  ( -47.59344166597622916, -24.15620529776627379, 10.23563542870660825 ) ) ;
#63572=ORIENTED_EDGE ( 'NONE', *, *, #91723, .T. ) ;
#63574=CARTESIAN_POINT ( 'NONE',  ( -120.6228709571501128, -24.63345952396256422, 9.038047939301506517 ) ) ;
#63576=VERTEX_POINT ( 'NONE', #86001 ) ;
#63577=CARTESIAN_POINT ( 'NONE',  ( -39.58953762381673158, -24.66019654487199375, 8.947790411086133489 ) ) ;
#63578=EDGE_LOOP ( 'NONE', ( #82520, #45990, #61671, #78920 ) ) ;
#63580=CARTESIAN_POINT ( 'NONE',  ( -107.6228709571500701, -23.47593901973091235, -1.443836447538999312 ) ) ;
#63581=CARTESIAN_POINT ( 'NONE',  ( -19.96038302963917488, -7.207760892512529161, -1.500000000000002220 ) ) ;
#63583=CARTESIAN_POINT ( 'NONE',  ( -50.59279366430950375, -24.40034930558991277, 0.3402023900116070698 ) ) ;
#63585=CARTESIAN_POINT ( 'NONE',  ( 18.38516380405726736, -11.72527425286322611, -1.500000000000002220 ) ) ;
#63586=CARTESIAN_POINT ( 'NONE',  ( -103.6288238165831075, -24.15620529776628445, 10.23563542870660292 ) ) ;
#63588=CARTESIAN_POINT ( 'NONE',  ( -109.5228709571500616, -24.65952944569305316, 1.056160979905704123 ) ) ;
#63589=CARTESIAN_POINT ( 'NONE',  ( -20.50126671893153940, -7.481214725051755110, -1.500000000000002220 ) ) ;
#63593=CARTESIAN_POINT ( 'NONE',  ( -85.52211221999672830, -23.48786465467240703, 11.44779295918254647 ) ) ;
#63597=DIRECTION ( 'NONE',  ( 3.773278334444167608E-23, -1.000000000000000000, 0.000000000000000000 ) ) ;
#63598=CARTESIAN_POINT ( 'NONE',  ( -82.50296107429853976, -24.51314013834315375, 0.6176544820404155089 ) ) ;
#63599=CARTESIAN_POINT ( 'NONE',  ( -7.948041996521916452, 19.69052605537007850, -1.500000000000002220 ) ) ;
#63600=AXIS2_PLACEMENT_3D ( 'NONE', #40291, #78334, #55022 ) ;
#63601=CARTESIAN_POINT ( 'NONE',  ( -94.54705908665695802, -24.51314013834316086, 0.6176544820404165081 ) ) ;
#63602=CARTESIAN_POINT ( 'NONE',  ( -30.60464735295150263, -24.58764167366260622, 9.439037205594624780 ) ) ;
#63604=CARTESIAN_POINT ( 'NONE',  ( -44.58953762381671737, -23.48786465467240347, 11.44779295918255180 ) ) ;
#63606=CARTESIAN_POINT ( 'NONE',  ( 19.37663158793545293, -0.8356294931911363300, 11.49999999999998934 ) ) ;
#63608=CARTESIAN_POINT ( 'NONE',  ( -45.47736248591412078, -24.83618233451449697, 1.606449574219536158 ) ) ;
#63609=ORIENTED_EDGE ( 'NONE', *, *, #43528, .F. ) ;
#63610=CARTESIAN_POINT ( 'NONE',  ( 7.694069055508638399, 17.95645395709951941, 11.49999999999999645 ) ) ;
#63612=CARTESIAN_POINT ( 'NONE',  ( -68.52287095715006160, -24.64898659630528854, 1.056161002820824368 ) ) ;
#63615=CARTESIAN_POINT ( 'NONE',  ( -51.52764846858840997, -25.24768739062223943, 6.187572788000800017 ) ) ;
#63618=CARTESIAN_POINT ( 'NONE',  ( -101.1977347980315329, -25.23200539837010936, 3.666257912286023490 ) ) ;
#63619=CARTESIAN_POINT ( 'NONE',  ( -19.67010641940559168, 0.002901314006966619011, 11.49999999999998934 ) ) ;
#63620=B_SPLINE_CURVE_WITH_KNOTS ( 'NONE', 3,
 ( #25236, #93745, #15620, #77512, #56212, #38962 ),
 .UNSPECIFIED., .F., .F.,
 ( 4, 2, 4 ),
 ( 6.384118696083428989E-06, 0.001386860460837108884, 0.002767336802978134086 ),
 .UNSPECIFIED. ) ;
#63622=ORIENTED_EDGE ( 'NONE', *, *, #81511, .T. ) ;
#63623=CARTESIAN_POINT ( 'NONE',  ( -90.52287095715001897, -24.15516710230294350, 10.28746687063725851 ) ) ;
#63624=CARTESIAN_POINT ( 'NONE',  ( -43.58953762381671737, -24.64898659630367206, 1.056161002820379169 ) ) ;
#63626=VECTOR ( 'NONE', #91782, 1000.000000000000114 ) ;
#63630=CARTESIAN_POINT ( 'NONE',  ( -97.51358029338079803, -24.15620529776628800, 10.23563542870660115 ) ) ;
#63633=CARTESIAN_POINT ( 'NONE',  ( -129.5557419245657513, -24.51314013834316796, 0.6176544820404223923 ) ) ;
#63635=CARTESIAN_POINT ( 'NONE',  ( -114.5930451687649168, -23.73791477778912551, 11.05961554403169878 ) ) ;
#63636=CARTESIAN_POINT ( 'NONE',  ( -12.53609265798794681, -15.47265773855268378, 11.49999999999998934 ) ) ;
#63637=CARTESIAN_POINT ( 'NONE',  ( -75.62719797981144154, -24.83644354573578994, 8.397322867130100121 ) ) ;
#63638=CARTESIAN_POINT ( 'NONE',  ( -19.78623529325263775, -1.157695164950638844, -1.500000000000002220 ) ) ;
#63640=CARTESIAN_POINT ( 'NONE',  ( -90.25931493494785229, -25.32787839792626627, 4.644810655877241956 ) ) ;
#63641=CARTESIAN_POINT ( 'NONE',  ( -104.6228709571500417, -23.72773821059535848, 11.05748984161097503 ) ) ;
#63642=CARTESIAN_POINT ( 'NONE',  ( -95.52287095715004739, -23.47593901973090169, -1.443836447538996648 ) ) ;
#63643=CARTESIAN_POINT ( 'NONE',  ( -4.968023186724614959, -20.10795263665959709, 11.49999999999999645 ) ) ;
#63644=DIRECTION ( 'NONE',  ( 1.000000000000000000, 3.773278334444167608E-23, 8.201307816334959825E-29 ) ) ;
#63645=CARTESIAN_POINT ( 'NONE',  ( -126.5228709571500616, -24.64898659630368627, 1.056161002820834804 ) ) ;
#63646=CARTESIAN_POINT ( 'NONE',  ( 4.306090731860143350, 22.38281141545218844, 11.49999999999999645 ) ) ;
#63648=B_SPLINE_CURVE_WITH_KNOTS ( 'NONE', 3,
 ( #85999, #9369, #62178, #63690 ),
 .UNSPECIFIED., .F., .F.,
 ( 4, 4 ),
 ( 0.3089841683514000792, 0.3099849153921654943 ),
 .UNSPECIFIED. ) ;
#63650=B_SPLINE_SURFACE_WITH_KNOTS ( 'NONE', 3, 3, ( 
 ( #45931, #44937, #60168, #61660 ),
 ( #5859, #36816, #75859, #6854 ),
 ( #30183, #77349, #7343, #38298 ),
 ( #69254, #91090, #13961, #13461 ),
 ( #92578, #6362, #38798, #100173 ),
 ( #37319, #52538, #31182, #93079 ),
 ( #23564, #82971, #44435, #87478 ) ),
 .UNSPECIFIED., .F., .F., .F.,
 ( 4, 3, 4 ),
 ( 4, 4 ),
 ( 0.0004766839783823623123, 0.1029713700210900668, 0.2054660560637977806 ),
 ( 0.06951167983181827381, 0.07055647694920491597 ),
 .UNSPECIFIED. ) ;
#63651=CARTESIAN_POINT ( 'NONE',  ( -69.59246360937903830, -24.15543982623907127, -0.2315651400026648155 ) ) ;
#63652=FACE_OUTER_BOUND ( 'NONE', #48094, .T. ) ;
#63654=CARTESIAN_POINT ( 'NONE',  ( -20.14672940031187665, -1.731937678239350298, -1.500000000000002220 ) ) ;
#63655=B_SPLINE_CURVE_WITH_KNOTS ( 'NONE', 3,
 ( #52882, #37148, #68111, #77191 ),
 .UNSPECIFIED., .F., .F.,
 ( 4, 4 ),
 ( 0.000000000000000000, 9.999999999997510880E-05 ),
 .UNSPECIFIED. ) ;
#63656=LINE ( 'NONE', #40795, #22526 ) ;
#63658=EDGE_CURVE ( 'NONE', #28945, #58432, #23585, .T. ) ;
#63661=DIRECTION ( 'NONE',  ( -1.000000000000000000, -3.773278334444167608E-23, -8.201307833595939069E-29 ) ) ;
#63662=CARTESIAN_POINT ( 'NONE',  ( -14.98413761715186077, 17.36544542080599740, -1.500000000000002220 ) ) ;
#63664=CARTESIAN_POINT ( 'NONE',  ( 11.47056939498152950, -16.38825109899074661, -1.500000000000002220 ) ) ;
#63665=CARTESIAN_POINT ( 'NONE',  ( -41.26959558397307148, -25.08918874615346439, 7.338714959427068862 ) ) ;
#63668=CARTESIAN_POINT ( 'NONE',  ( 10.03794737889396771, 18.37758748099471973, 11.49999999999999645 ) ) ;
#63669=CARTESIAN_POINT ( 'NONE',  ( -28.89996118126751767, -24.85249319229149023, 7.829856784274641157 ) ) ;
#63671=CARTESIAN_POINT ( 'NONE',  ( -5.561696574893697509, -21.35426480686918538, 11.49999999999998934 ) ) ;
#63672=EDGE_CURVE ( 'NONE', #65405, #47332, #7874, .T. ) ;
#63673=B_SPLINE_CURVE_WITH_KNOTS ( 'NONE', 3,
 ( #14853, #7241, #85367, #38192 ),
 .UNSPECIFIED., .F., .F.,
 ( 4, 4 ),
 ( 2.775557561562891351E-17, 9.999999999998898659E-05 ),
 .UNSPECIFIED. ) ;
#63676=CARTESIAN_POINT ( 'NONE',  ( -60.52287095715006870, -24.62226745350439217, 0.9660975649728013037 ) ) ;
#63677=CARTESIAN_POINT ( 'NONE',  ( -49.73776537321236901, -25.27344806511582576, 3.509878174495147274 ) ) ;
#63681=ORIENTED_EDGE ( 'NONE', *, *, #89345, .T. ) ;
#63682=VERTEX_POINT ( 'NONE', #85494 ) ;
#63684=CARTESIAN_POINT ( 'NONE',  ( -100.4784170818037552, -25.10935802628761948, 2.833156094507327083 ) ) ;
#63685=CARTESIAN_POINT ( 'NONE',  ( -90.70643023311484399, -25.31959457942835456, 5.296252855621696121 ) ) ;
#63686=EDGE_CURVE ( 'NONE', #53182, #77233, #16841, .T. ) ;
#63687=CARTESIAN_POINT ( 'NONE',  ( 3.262959013008915665, -20.29835246810489835, -1.500000000000002220 ) ) ;
#63688=B_SPLINE_CURVE_WITH_KNOTS ( 'NONE', 3,
 ( #43560, #26831, #89733, #33948, #74497, #4504, #4991, #88740 ),
 .UNSPECIFIED., .F., .F.,
 ( 4, 2, 2, 4 ),
 ( 0.000000000000000000, 0.002001098010032801612, 0.003001647015049202418, 0.004002196020065603224 ),
 .UNSPECIFIED. ) ;
#63689=ORIENTED_EDGE ( 'NONE', *, *, #100021, .T. ) ;
#63690=CARTESIAN_POINT ( 'NONE',  ( -61.62287095715004881, -23.47596703998600631, 11.44779298504227505 ) ) ;
#63691=CARTESIAN_POINT ( 'NONE',  ( -44.48280314835779592, -24.65952944569304606, 1.056160979905693909 ) ) ;
#63693=CARTESIAN_POINT ( 'NONE',  ( -20.85237562250380350, -7.973873963886685345, -1.500000000000002220 ) ) ;
#63694=B_SPLINE_CURVE_WITH_KNOTS ( 'NONE', 3,
 ( #12042, #43012, #87680, #4450 ),
 .UNSPECIFIED., .F., .F.,
 ( 4, 4 ),
 ( 0.8511077552149090009, 0.8601141864870244236 ),
 .UNSPECIFIED. ) ;
#63696=CARTESIAN_POINT ( 'NONE',  ( -0.008164624327092535883, -22.94430252198347020, 6.147794833475638043 ) ) ;
#63697=PLANE ( 'NONE',  #25308 ) ;
#63700=CARTESIAN_POINT ( 'NONE',  ( -124.6228709571500559, -24.64898659630368627, 1.056161002820833028 ) ) ;
#63702=CARTESIAN_POINT ( 'NONE',  ( 3.748101851616784774, 20.49759516964078188, -1.500000000000002220 ) ) ;
#63704=CARTESIAN_POINT ( 'NONE',  ( -52.52287095715004739, -23.73907113217698495, -1.053371485780741024 ) ) ;
#63707=VECTOR ( 'NONE', #98288, 1000.000000000000114 ) ;
#63708=CARTESIAN_POINT ( 'NONE',  ( -69.33560399441930144, -25.03149286552998376, 7.166139700104196208 ) ) ;
#63709=CARTESIAN_POINT ( 'NONE',  ( -13.06023916655064276, -16.53025015627232719, -1.500000000000002220 ) ) ;
#63711=CARTESIAN_POINT ( 'NONE',  ( -37.58953762381673158, -24.64965694238406968, 8.947790433994661896 ) ) ;
#63712=CARTESIAN_POINT ( 'NONE',  ( -37.52287095715009713, -23.95044443724992789, 10.65354141964649237 ) ) ;
#63713=PLANE ( 'NONE',  #93446 ) ;
#63715=CARTESIAN_POINT ( 'NONE',  ( -86.50735162477467100, -24.35071581493543391, 9.817618358456027039 ) ) ;
#63716=DIRECTION ( 'NONE',  ( -3.773278334444166432E-23, 1.000000000000000000, 0.000000000000000000 ) ) ;
#63717=DIRECTION ( 'NONE',  ( -3.773278334453079030E-23, 0.9999999999976377785, 2.173523156925979128E-06 ) ) ;
#63719=CARTESIAN_POINT ( 'NONE',  ( 13.39142644571787422, -17.71860720625715757, 11.49999999999999645 ) ) ;
#63723=ORIENTED_EDGE ( 'NONE', *, *, #67809, .F. ) ;
#63724=CARTESIAN_POINT ( 'NONE',  ( -12.60694655700363143, 18.86142483545513926, -1.500000000000002220 ) ) ;
#63725=CARTESIAN_POINT ( 'NONE',  ( -118.6228709571500275, -23.72773821059536559, 11.05748984161097681 ) ) ;
#63726=EDGE_LOOP ( 'NONE', ( #90403, #5034, #28699, #81005 ) ) ;
#63727=EDGE_CURVE ( 'NONE', #34154, #48223, #35011, .T. ) ;
#63730=ADVANCED_FACE ( 'NONE', ( #93181 ), #53647, .F. ) ;
#63731=CARTESIAN_POINT ( 'NONE',  ( 13.66866334921533799, -14.80927461459226890, -1.500000000000002220 ) ) ;
#63732=B_SPLINE_CURVE_WITH_KNOTS ( 'NONE', 3,
 ( #37007, #98896, #29390, #91293 ),
 .UNSPECIFIED., .F., .F.,
 ( 4, 4 ),
 ( 0.000000000000000000, 9.999999999996123101E-05 ),
 .UNSPECIFIED. ) ;
#63733=CARTESIAN_POINT ( 'NONE',  ( -83.62287095715007013, -23.47596703998600631, 11.44779298504227860 ) ) ;
#63736=CARTESIAN_POINT ( 'NONE',  ( -22.41777205227948855, 0.6913007675000180097, -1.500000000000002220 ) ) ;
#63737=ORIENTED_EDGE ( 'NONE', *, *, #44083, .F. ) ;
#63738=EDGE_LOOP ( 'NONE', ( #26734, #21698, #49571, #55385 ) ) ;
#63739=FACE_OUTER_BOUND ( 'NONE', #86030, .T. ) ;
#63741=CARTESIAN_POINT ( 'NONE',  ( -48.58953762381672448, -24.66019654487199375, 8.947790411086138818 ) ) ;
#63743=DIRECTION ( 'NONE',  ( -3.773278334453079030E-23, 0.9999999999976377785, 2.173523156925979128E-06 ) ) ;
#63745=CARTESIAN_POINT ( 'NONE',  ( -16.13938233076020268, 11.07636124087057183, -1.500000000000002220 ) ) ;
#63747=DIRECTION ( 'NONE',  ( 0.000000000000000000, -2.173523156925980399E-06, 0.9999999999976378895 ) ) ;
#63749=CARTESIAN_POINT ( 'NONE',  ( 11.78165356204951131, -17.99452314462042324, 11.49999999999998934 ) ) ;
#63750=CARTESIAN_POINT ( 'NONE',  ( -94.62287095715005592, -29.50248528299804818, 1.056150453629040253 ) ) ;
#63753=CARTESIAN_POINT ( 'NONE',  ( -80.62287095715001328, -24.14406661707769075, 10.28769366152060627 ) ) ;
#63754=CARTESIAN_POINT ( 'NONE',  ( 22.43992371924722917, 4.826111843257130829, -1.500000000000002220 ) ) ;
#63758=DIRECTION ( 'NONE',  ( 0.000000000000000000, -2.173523156925980399E-06, 0.9999999999976378895 ) ) ;
#63759=CARTESIAN_POINT ( 'NONE',  ( 17.67427751897593069, 9.450557017276361549, 11.49999999999999645 ) ) ;
#63761=CARTESIAN_POINT ( 'NONE',  ( -113.5895376238167245, -24.64965694238408034, 8.947790433994653014 ) ) ;
#63762=CARTESIAN_POINT ( 'NONE',  ( -46.52287095715004028, -23.73907113216989373, -1.053371485793254125 ) ) ;
#63764=CARTESIAN_POINT ( 'NONE',  ( -85.62287095715011276, -24.82558206586144323, 1.605769216559442158 ) ) ;
#63765=CARTESIAN_POINT ( 'NONE',  ( 19.41305359857673096, 4.112862643401165919, -1.500000000000002220 ) ) ;
#63766=CARTESIAN_POINT ( 'NONE',  ( -17.16505717403991227, -13.39166244882208012, 11.49999999999998934 ) ) ;
#63767=EDGE_CURVE ( 'NONE', #44470, #84523, #85858, .T. ) ;
#63769=CARTESIAN_POINT ( 'NONE',  ( -15.16444148636751521, -12.51942901160708921, -1.500000000000002220 ) ) ;
#63771=AXIS2_PLACEMENT_3D ( 'NONE', #79290, #15890, #63597 ) ;
#63772=CARTESIAN_POINT ( 'NONE',  ( -32.52287095715004739, -23.47593901973090169, -1.443836447538997092 ) ) ;
#63776=CARTESIAN_POINT ( 'NONE',  ( 20.53815866822273861, -0.6333348845813139283, 11.49999999999999645 ) ) ;
#63778=CARTESIAN_POINT ( 'NONE',  ( -120.6279586782334405, -23.85016227208581441, -0.8807180028928249804 ) ) ;
#63780=CARTESIAN_POINT ( 'NONE',  ( -21.70561270324154179, 6.225854807558039994, 11.49999999999999645 ) ) ;
#63781=ORIENTED_EDGE ( 'NONE', *, *, #91916, .F. ) ;
#63782=CARTESIAN_POINT ( 'NONE',  ( -70.32380231474228083, -25.25639601488367703, 7.101635269074562551 ) ) ;
#63785=CARTESIAN_POINT ( 'NONE',  ( -72.62287095715007013, -24.33927499327854704, 9.819080762295818943 ) ) ;
#63788=CARTESIAN_POINT ( 'NONE',  ( -25.68888630310901178, -24.61459721658222222, 6.447530656637062485 ) ) ;
#63789=DIRECTION ( 'NONE',  ( 0.5646109999446368155, 0.000000000000000000, -0.8253571461746226356 ) ) ;
#63791=CARTESIAN_POINT ( 'NONE',  ( 22.67273400128462058, 4.441195646929153362, 11.49999999999999645 ) ) ;
#63792=CARTESIAN_POINT ( 'NONE',  ( 9.452765381649220089, 20.79790602042944414, -1.500000000000002220 ) ) ;
#63794=DIRECTION ( 'NONE',  ( 0.000000000000000000, 2.173523156925980399E-06, -0.9999999999976378895 ) ) ;
#63795=CARTESIAN_POINT ( 'NONE',  ( -82.62360247695944793, -24.66019654487199730, 8.947790411086122830 ) ) ;
#63796=ADVANCED_FACE ( 'NONE', ( #8455 ), #6977, .T. ) ;
#63797=CARTESIAN_POINT ( 'NONE',  ( -18.88510386880526326, 12.19974334031638641, 11.49999999999999645 ) ) ;
#63800=CARTESIAN_POINT ( 'NONE',  ( 21.92589416912191069, -1.073809401359021143, 11.49999999999998934 ) ) ;
#63801=ADVANCED_FACE ( 'NONE', ( #9454 ), #40411, .F. ) ;
#63802=CARTESIAN_POINT ( 'NONE',  ( -124.4728709571500360, -25.40558663563427189, 5.000950442582704270 ) ) ;
#63803=CARTESIAN_POINT ( 'NONE',  ( -34.64252832595930442, -24.15620529776627379, 10.23563542870661003 ) ) ;
#63805=VERTEX_POINT ( 'NONE', #43782 ) ;
#63806=CARTESIAN_POINT ( 'NONE',  ( -64.62287095715005592, -24.64898659630528499, 1.056161002820822592 ) ) ;
#63808=ORIENTED_EDGE ( 'NONE', *, *, #10142, .T. ) ;
#63809=CARTESIAN_POINT ( 'NONE',  ( -18.82070947631147106, 8.064391923812276985, -1.500000000000002220 ) ) ;
#63811=EDGE_LOOP ( 'NONE', ( #42595, #76507, #12383, #74169 ) ) ;
#63813=EDGE_LOOP ( 'NONE', ( #3295, #67689, #94384, #95005 ) ) ;
#63814=CARTESIAN_POINT ( 'NONE',  ( 13.31140876108729998, -18.89465134148960956, 11.49999999999998934 ) ) ;
#63815=PLANE ( 'NONE',  #3369 ) ;
#63817=CARTESIAN_POINT ( 'NONE',  ( 15.76184642470745700, 12.85868457875834103, -1.500000000000002220 ) ) ;
#63819=ORIENTED_EDGE ( 'NONE', *, *, #8693, .F. ) ;
#63820=CARTESIAN_POINT ( 'NONE',  ( -103.6228709571500559, -29.50250243563736774, 8.947779886222138046 ) ) ;
#63822=CARTESIAN_POINT ( 'NONE',  ( -44.52287095715007581, -24.66019654487199730, 8.947790411086117501 ) ) ;
#63824=CARTESIAN_POINT ( 'NONE',  ( 2.564635614221720594, -21.35862533600356983, 11.49999999999999645 ) ) ;
#63825=ORIENTED_EDGE ( 'NONE', *, *, #71348, .F. ) ;
#63826=CARTESIAN_POINT ( 'NONE',  ( -75.54455309653219786, -24.52300882791530157, 0.6510814631126414787 ) ) ;
#63827=B_SPLINE_CURVE_WITH_KNOTS ( 'NONE', 3,
 ( #46303, #77230, #7738, #62039, #92965, #23440, #626, #2646 ),
 .UNSPECIFIED., .F., .F.,
 ( 4, 2, 2, 4 ),
 ( -0.001224554619866348015, -0.0002241820295893657503, 0.0007761905606876165140, 0.002776935741241576706 ),
 .UNSPECIFIED. ) ;
#63831=CARTESIAN_POINT ( 'NONE',  ( 12.20387445076365296, 16.77033177596414504, -1.500000000000002220 ) ) ;
#63832=ORIENTED_EDGE ( 'NONE', *, *, #55520, .T. ) ;
#63834=ORIENTED_EDGE ( 'NONE', *, *, #80825, .T. ) ;
#63836=CARTESIAN_POINT ( 'NONE',  ( -129.6228709571500417, -23.47596703998600631, 11.44779298504227683 ) ) ;
#63838=ORIENTED_EDGE ( 'NONE', *, *, #53083, .F. ) ;
#63839=CARTESIAN_POINT ( 'NONE',  ( -28.55620429048338949, -24.50218025470241301, 8.947790429581973015 ) ) ;
#63840=CARTESIAN_POINT ( 'NONE',  ( -42.48186235109157138, -24.66019654487198665, 8.947790411086131712 ) ) ;
#63841=CARTESIAN_POINT ( 'NONE',  ( -65.62287095715005592, -24.99132157543084176, 2.256160258750667502 ) ) ;
#63842=CARTESIAN_POINT ( 'NONE',  ( 21.52718982488130450, -4.553922534329950089, 11.49999999999999645 ) ) ;
#63844=CARTESIAN_POINT ( 'NONE',  ( -103.5888980205460257, -24.34968618360933945, 0.1864209137778842229 ) ) ;
#63845=CARTESIAN_POINT ( 'NONE',  ( -16.99934442671578694, -14.85117937636706031, -1.500000000000002220 ) ) ;
#63846=CARTESIAN_POINT ( 'NONE',  ( 17.27681320446407298, 11.92757687370068886, 11.49999999999998934 ) ) ;
#63847=FACE_OUTER_BOUND ( 'NONE', #47298, .T. ) ;
#63849=EDGE_LOOP ( 'NONE', ( #56583, #4506, #89198, #70628 ) ) ;
#63853=CARTESIAN_POINT ( 'NONE',  ( -57.62367090558025495, -24.66019654487199375, 8.947790411086119278 ) ) ;
#63854=ORIENTED_EDGE ( 'NONE', *, *, #20908, .F. ) ;
#63855=CARTESIAN_POINT ( 'NONE',  ( 16.66693084842116335, 13.01107939256401913, 11.49999999999998934 ) ) ;
#63856=CARTESIAN_POINT ( 'NONE',  ( -82.62287095715005592, -24.65952944569304606, 1.056160979905699016 ) ) ;
#63857=CARTESIAN_POINT ( 'NONE',  ( -59.79157152756309301, -25.29489609436097552, 6.057563354383566967 ) ) ;
#63858=CARTESIAN_POINT ( 'NONE',  ( -75.62287095715008434, -24.62226745350437440, 0.9660975649728090753 ) ) ;
#63860=CARTESIAN_POINT ( 'NONE',  ( -101.5228709571500900, -23.48783264082477018, -1.443836473390087249 ) ) ;
#63861=CARTESIAN_POINT ( 'NONE',  ( 17.07819277939130842, -14.19623557145530057, -1.500000000000002220 ) ) ;
#63862=VECTOR ( 'NONE', #64379, 1000.000000000000114 ) ;
#63863=CARTESIAN_POINT ( 'NONE',  ( -114.5930436926616949, -23.73766607897672287, -1.055555164236428700 ) ) ;
#63864=B_SPLINE_CURVE_WITH_KNOTS ( 'NONE', 3,
 ( #97906, #66993, #20778, #7067, #67984, #99408 ),
 .UNSPECIFIED., .F., .F.,
 ( 4, 2, 4 ),
 ( 0.000000000000000000, 0.001380764517854763014, 0.002761529035709526028 ),
 .UNSPECIFIED. ) ;
#63865=ORIENTED_EDGE ( 'NONE', *, *, #80626, .T. ) ;
#63867=CARTESIAN_POINT ( 'NONE',  ( -58.52287095715006160, -23.47596703998600631, 11.44779298504228926 ) ) ;
#63868=CARTESIAN_POINT ( 'NONE',  ( -126.5218661376151488, -23.73766607897670511, -1.055555164236450238 ) ) ;
#63869=CARTESIAN_POINT ( 'NONE',  ( -36.62372838562182409, -24.66019654487199730, 8.947790411086113949 ) ) ;
#63870=CARTESIAN_POINT ( 'NONE',  ( 0.2958748881272694198, 19.47992435465491212, 11.49999999999998934 ) ) ;
#63871=CARTESIAN_POINT ( 'NONE',  ( -16.30254408640404051, -13.89340296626662230, -1.500000000000002220 ) ) ;
#63872=CARTESIAN_POINT ( 'NONE',  ( -85.52287095715006160, -23.47596703998600631, 11.44779298504228393 ) ) ;
#63873=DIRECTION ( 'NONE',  ( -1.000000000000000000, -3.773278334444167608E-23, -8.201307833595939069E-29 ) ) ;
#63874=CARTESIAN_POINT ( 'NONE',  ( -51.60611487679543785, -23.73766607897669445, -1.055555164236457788 ) ) ;
#63875=CARTESIAN_POINT ( 'NONE',  ( -77.60072041985134206, -23.73766607897670156, -1.055555164236459564 ) ) ;
#63876=CARTESIAN_POINT ( 'NONE',  ( 22.69831151501224298, -1.600861625767590724, -1.500000000000002220 ) ) ;
#63877=B_SPLINE_CURVE_WITH_KNOTS ( 'NONE', 3,
 ( #45577, #7496, #66924, #97843 ),
 .UNSPECIFIED., .F., .F.,
 ( 4, 4 ),
 ( 0.000000000000000000, 9.999999999998897304E-05 ),
 .UNSPECIFIED. ) ;
#63878=EDGE_CURVE ( 'NONE', #12512, #41731, #72581, .T. ) ;
#63879=CARTESIAN_POINT ( 'NONE',  ( -106.5486680884517199, -24.66019654487200441, 8.947790411086108620 ) ) ;
#63881=CARTESIAN_POINT ( 'NONE',  ( 3.337697395173636394, -19.57427954046807983, 11.49999999999999645 ) ) ;
#63884=CARTESIAN_POINT ( 'NONE',  ( -103.5228709571500758, -24.64898659630367916, 1.056161002820829697 ) ) ;
#63886=EDGE_LOOP ( 'NONE', ( #72256, #17365, #16022, #80883 ) ) ;
#63887=CARTESIAN_POINT ( 'NONE',  ( -49.40445554211785151, -25.19972462862641294, 6.604535875143222157 ) ) ;
#63889=VECTOR ( 'NONE', #66418, 1000.000000000000114 ) ;
#63890=CARTESIAN_POINT ( 'NONE',  ( -63.52287095715006160, -23.48786465467241058, 11.44779295918254824 ) ) ;
#63891=CARTESIAN_POINT ( 'NONE',  ( -20.76051858633888259, -6.224802954461835292, 11.49999999999998934 ) ) ;
#63893=CARTESIAN_POINT ( 'NONE',  ( -50.88999612354844970, -25.05389627988721202, 7.512545578324246520 ) ) ;
#63894=CARTESIAN_POINT ( 'NONE',  ( -19.16120753946698585, -3.443109951913609024, -1.500000000000002220 ) ) ;
#63896=CARTESIAN_POINT ( 'NONE',  ( -55.57991466617167475, -24.83644354573578283, 8.397322867130093016 ) ) ;
#63897=B_SPLINE_CURVE_WITH_KNOTS ( 'NONE', 3,
 ( #63400, #65408, #72004, #95327 ),
 .UNSPECIFIED., .F., .F.,
 ( 4, 4 ),
 ( 0.000000000000000000, 9.999999999998897304E-05 ),
 .UNSPECIFIED. ) ;
#63898=VERTEX_POINT ( 'NONE', #17567 ) ;
#63901=CARTESIAN_POINT ( 'NONE',  ( -0.9335293527496063559, -20.33857301660709638, 11.49999999999999645 ) ) ;
#63902=CARTESIAN_POINT ( 'NONE',  ( -35.62287095715005592, -24.99156045073392463, 7.747789690856161648 ) ) ;
#63905=LINE ( 'NONE', #70996, #23235 ) ;
#63908=DIRECTION ( 'NONE',  ( -0.000000000000000000, 2.173523156925979552E-06, -0.9999999999976378895 ) ) ;
#63909=CARTESIAN_POINT ( 'NONE',  ( -86.52287095715004739, -24.34917612407046761, 0.1852690917481102650 ) ) ;
#63910=EDGE_CURVE ( 'NONE', #68524, #57335, #81023, .T. ) ;
#63911=LINE ( 'NONE', #41049, #72759 ) ;
#63912=ORIENTED_EDGE ( 'NONE', *, *, #40256, .T. ) ;
#63914=CARTESIAN_POINT ( 'NONE',  ( 16.23347398924790497, -16.23827457187686463, 11.49999999999999645 ) ) ;
#63915=CARTESIAN_POINT ( 'NONE',  ( 12.47407908559008760, -19.03963781694049473, 11.49999999999998934 ) ) ;
#63917=CARTESIAN_POINT ( 'NONE',  ( -30.47287095715006799, -24.98489225261240065, 7.794711013822600343 ) ) ;
#63918=LINE ( 'NONE', #72015, #18782 ) ;
#63919=CARTESIAN_POINT ( 'NONE',  ( -81.52287095715006160, -23.95044443724992789, 10.65354141964649415 ) ) ;
#63920=CARTESIAN_POINT ( 'NONE',  ( -31.52287095715006160, -29.50250243563736774, 8.947779886222150481 ) ) ;
#63922=CARTESIAN_POINT ( 'NONE',  ( -69.65142986114982193, -23.48786465467240703, 11.44779295918255002 ) ) ;
#63923=EDGE_CURVE ( 'NONE', #28525, #73391, #38594, .T. ) ;
#63924=B_SPLINE_CURVE_WITH_KNOTS ( 'NONE', 3,
 ( #71873, #58150, #65777, #3373, #11461, #42926 ),
 .UNSPECIFIED., .F., .F.,
 ( 4, 2, 4 ),
 ( 1.570755371634494188E-05, 0.001396183895866093174, 0.002776660238015841650 ),
 .UNSPECIFIED. ) ;
#63927=CARTESIAN_POINT ( 'NONE',  ( -99.14000973721185517, -25.25460558555856494, 5.341016530524719919 ) ) ;
#63928=EDGE_LOOP ( 'NONE', ( #46083, #61090, #83072, #79411 ) ) ;
#63929=B_SPLINE_CURVE_WITH_KNOTS ( 'NONE', 3,
 ( #87312, #66011, #87822, #42664 ),
 .UNSPECIFIED., .F., .F.,
 ( 4, 4 ),
 ( 0.000000000000000000, 9.999999999998900014E-05 ),
 .UNSPECIFIED. ) ;
#63930=CARTESIAN_POINT ( 'NONE',  ( 7.100489274569507181, 19.11111018586187527, 11.49999999999998934 ) ) ;
#63932=B_SPLINE_CURVE_WITH_KNOTS ( 'NONE', 3,
 ( #18259, #19740, #50713, #81662 ),
 .UNSPECIFIED., .F., .F.,
 ( 4, 4 ),
 ( 0.000000000000000000, 0.001261718750000001554 ),
 .UNSPECIFIED. ) ;
#63934=CARTESIAN_POINT ( 'NONE',  ( 10.47623847176155820, -20.49086732513842080, -1.500000000000002220 ) ) ;
#63935=DIRECTION ( 'NONE',  ( -3.773278334453079618E-23, 0.9999999999976377785, 2.173523156925979975E-06 ) ) ;
#63936=EDGE_CURVE ( 'NONE', #27060, #68434, #71867, .T. ) ;
#63937=ORIENTED_EDGE ( 'NONE', *, *, #5, .F. ) ;
#63938=CARTESIAN_POINT ( 'NONE',  ( -108.5181428159692558, -23.96169478059714564, 10.65365249895716993 ) ) ;
#63940=EDGE_CURVE ( 'NONE', #10349, #26640, #82271, .T. ) ;
#63941=EDGE_CURVE ( 'NONE', #27148, #30482, #41133, .T. ) ;
#63942=CARTESIAN_POINT ( 'NONE',  ( -78.62287095715005592, -24.64965695001468404, 8.947790433994182280 ) ) ;
#63943=CARTESIAN_POINT ( 'NONE',  ( -53.62368185415960653, -24.66019654487199375, 8.947790411086122830 ) ) ;
#63944=CARTESIAN_POINT ( 'NONE',  ( -19.36244235409943926, 8.944087295975924334, 11.49999999999999645 ) ) ;
#63945=ORIENTED_EDGE ( 'NONE', *, *, #87373, .F. ) ;
#63946=EDGE_LOOP ( 'NONE', ( #16231, #30320, #32833, #33552 ) ) ;
#63947=CARTESIAN_POINT ( 'NONE',  ( 1.019757120859956512, 22.21710203930399175, 11.49999999999998934 ) ) ;
#63948=CARTESIAN_POINT ( 'NONE',  ( -17.42616458466809704, -11.11377323884725321, -1.500000000000002220 ) ) ;
#63952=CARTESIAN_POINT ( 'NONE',  ( -95.58514779555582663, -24.83644354573579349, 8.397322867130096569 ) ) ;
#63953=ORIENTED_EDGE ( 'NONE', *, *, #55091, .T. ) ;
#63954=CARTESIAN_POINT ( 'NONE',  ( -127.5895376238167245, -24.64898659630368627, 1.056161002820394046 ) ) ;
#63955=ORIENTED_EDGE ( 'NONE', *, *, #56483, .F. ) ;
#63956=CARTESIAN_POINT ( 'NONE',  ( -58.50332490849174150, -24.15620529776628089, 10.23563542870660470 ) ) ;
#63957=CARTESIAN_POINT ( 'NONE',  ( -70.90965497510502757, -25.15133953616122398, 6.934644986962871904 ) ) ;
#63958=CARTESIAN_POINT ( 'NONE',  ( -7.158894406585330827, 19.61798520005962487, -1.500000000000002220 ) ) ;
#63959=CARTESIAN_POINT ( 'NONE',  ( -19.11951126197014261, -10.51958540666066533, 11.49999999999999645 ) ) ;
#63960=VECTOR ( 'NONE', #73523, 1000.000000000000114 ) ;
#63961=CARTESIAN_POINT ( 'NONE',  ( -26.80323004365396145, -24.77993723737401766, 7.264871099892241446 ) ) ;
#63963=CARTESIAN_POINT ( 'NONE',  ( -15.60622653811170402, 16.18669697583415967, -1.500000000000002220 ) ) ;
#63964=CARTESIAN_POINT ( 'NONE',  ( -26.12923826827997686, -24.97066931972152304, 5.595194356714370265 ) ) ;
#63965=CARTESIAN_POINT ( 'NONE',  ( -72.52287095715010423, -23.96177878511308634, 10.65340807706330395 ) ) ;
#63968=VERTEX_POINT ( 'NONE', #41412 ) ;
#63969=ORIENTED_EDGE ( 'NONE', *, *, #59871, .F. ) ;
#63970=B_SPLINE_CURVE_WITH_KNOTS ( 'NONE', 3,
 ( #9860, #48436, #71267, #33705 ),
 .UNSPECIFIED., .F., .F.,
 ( 4, 4 ),
 ( 0.000000000000000000, 9.999999999998897304E-05 ),
 .UNSPECIFIED. ) ;
#63973=CARTESIAN_POINT ( 'NONE',  ( 1.185105815240312888, -21.37944065014308848, -1.500000000000002220 ) ) ;
#63974=CARTESIAN_POINT ( 'NONE',  ( -15.27869365379592281, -16.34152646814254339, 11.49999999999999645 ) ) ;
#63975=EDGE_LOOP ( 'NONE', ( #76014, #78636, #63221, #29027 ) ) ;
#63976=CARTESIAN_POINT ( 'NONE',  ( -82.52287095715006160, -23.47596703998600631, 11.44779298504228571 ) ) ;
#63977=CARTESIAN_POINT ( 'NONE',  ( 21.04674311342985860, -0.3259866984596996864, 11.49999999999998934 ) ) ;
#63978=CARTESIAN_POINT ( 'NONE',  ( -30.57662579376099288, -23.78795187145987100, 10.97490056816818971 ) ) ;
#63979=CARTESIAN_POINT ( 'NONE',  ( -18.69216024341242743, -6.879743215651725308, -1.500000000000002220 ) ) ;
#63980=CARTESIAN_POINT ( 'NONE',  ( -50.58553729207245908, -24.63419186844610564, 9.035850630976916875 ) ) ;
#63981=CARTESIAN_POINT ( 'NONE',  ( -80.48373552459977986, -25.30877073647739905, 4.508937044470972211 ) ) ;
#63982=CARTESIAN_POINT ( 'NONE',  ( 13.62230711432095553, -17.35066874027886286, -1.500000000000002220 ) ) ;
#63984=CARTESIAN_POINT ( 'NONE',  ( -65.49890678549689937, -24.40133493613049964, 9.663955038902802386 ) ) ;
#63985=B_SPLINE_CURVE_WITH_KNOTS ( 'NONE', 3,
 ( #66259, #26169, #79954, #56640, #97183, #65267 ),
 .UNSPECIFIED., .F., .F.,
 ( 4, 2, 4 ),
 ( 6.384118695039489680E-06, 0.001386860460836586732, 0.002767336802978133652 ),
 .UNSPECIFIED. ) ;
#63987=CARTESIAN_POINT ( 'NONE',  ( 20.25184064777635484, 4.944226511633750043, 11.49999999999999645 ) ) ;
#63989=FACE_OUTER_BOUND ( 'NONE', #15866, .T. ) ;
#63991=CARTESIAN_POINT ( 'NONE',  ( -56.62287095715005592, -23.48783264082478084, -1.443836473390068820 ) ) ;
#63992=CARTESIAN_POINT ( 'NONE',  ( -20.89022842043660688, 4.291957016416017900, 11.49999999999998934 ) ) ;
#63993=CARTESIAN_POINT ( 'NONE',  ( -97.62287095715009855, -23.96177878511308634, 10.65340807706329862 ) ) ;
#63994=CARTESIAN_POINT ( 'NONE',  ( -50.50967068900678925, -25.19546160786025979, 3.296984410641363716 ) ) ;
#63995=CARTESIAN_POINT ( 'NONE',  ( -71.58953762381673869, -24.65952944569304961, 1.056160979905698571 ) ) ;
#63996=CARTESIAN_POINT ( 'NONE',  ( -70.65510521343826156, -25.22594453560301631, 6.517383687127669134 ) ) ;
#63997=CARTESIAN_POINT ( 'NONE',  ( 7.090404290683943067, 21.45231405096426514, -1.500000000000002220 ) ) ;
#63999=DIRECTION ( 'NONE',  ( 1.000000000000000000, 3.773278334444167608E-23, 8.201307833595939069E-29 ) ) ;
#64001=CARTESIAN_POINT ( 'NONE',  ( -51.51942953060336805, -25.27075631336522221, 6.048200114948329542 ) ) ;
#64002=CARTESIAN_POINT ( 'NONE',  ( -31.55268919091492563, -23.96169478059712432, 10.65365249895719124 ) ) ;
#64003=CARTESIAN_POINT ( 'NONE',  ( 5.252985061998082017, 18.97096265210048571, 11.49999999999999645 ) ) ;
#64004=DIRECTION ( 'NONE',  ( 1.000000000000000000, 3.773278334444167608E-23, 8.201307833595939069E-29 ) ) ;
#64007=CARTESIAN_POINT ( 'NONE',  ( -99.62961886916561127, -24.15543982623907837, -0.2315651400026449425 ) ) ;
#64008=CARTESIAN_POINT ( 'NONE',  ( -55.62287095715002749, -24.14321612903111358, -0.2833117244521575206 ) ) ;
#64009=CARTESIAN_POINT ( 'NONE',  ( -124.6246528789468755, -24.15620529776629510, 10.23563542870659404 ) ) ;
#64015=EDGE_CURVE ( 'NONE', #95575, #5456, #45983, .T. ) ;
#64016=CARTESIAN_POINT ( 'NONE',  ( -19.06493894060550787, -22.58126814178390518, 11.44779298504228038 ) ) ;
#64017=CARTESIAN_POINT ( 'NONE',  ( 18.87426695099163254, 5.791883100666666451, -1.500000000000002220 ) ) ;
#64018=ORIENTED_EDGE ( 'NONE', *, *, #89778, .F. ) ;
#64019=EDGE_CURVE ( 'NONE', #77908, #90963, #76205, .T. ) ;
#64020=CARTESIAN_POINT ( 'NONE',  ( -9.806399893892750796, 17.69452640759178408, 11.49999999999999645 ) ) ;
#64023=VERTEX_POINT ( 'NONE', #62001 ) ;
#64024=CARTESIAN_POINT ( 'NONE',  ( -52.55620429048339304, -24.65952944569303895, 1.056160979905694575 ) ) ;
#64026=CARTESIAN_POINT ( 'NONE',  ( -100.3784397666924804, -25.03145178421234007, 7.561117244693161155 ) ) ;
#64027=CARTESIAN_POINT ( 'NONE',  ( -82.62287095715004170, -24.50216790748204332, 0.6166512839542541702 ) ) ;
#64028=FACE_OUTER_BOUND ( 'NONE', #29827, .T. ) ;
#64030=CARTESIAN_POINT ( 'NONE',  ( -3.121018476474317183, -19.76494895549465980, -1.500000000000002220 ) ) ;
#64031=EDGE_CURVE ( 'NONE', #39944, #5284, #7139, .T. ) ;
#64032=AXIS2_PLACEMENT_3D ( 'NONE', #57334, #56831, #18246 ) ;
#64033=CARTESIAN_POINT ( 'NONE',  ( -58.62287095715005592, -24.50216790748098461, 0.6166512839513552668 ) ) ;
#64034=CARTESIAN_POINT ( 'NONE',  ( -116.6285126153758682, -23.73791477778912551, 11.05961554403170055 ) ) ;
#64035=VERTEX_POINT ( 'NONE', #96 ) ;
#64036=EDGE_CURVE ( 'NONE', #36448, #40304, #94306, .T. ) ;
#64037=CARTESIAN_POINT ( 'NONE',  ( -79.50498077729714907, -24.35071581493543036, 9.817618358456028815 ) ) ;
#64038=CARTESIAN_POINT ( 'NONE',  ( -35.47955930521835910, -24.63355581998385091, 0.9682620441944008727 ) ) ;
#64039=CARTESIAN_POINT ( 'NONE',  ( -83.52287095715006160, -24.64898659630367916, 1.056161002820826145 ) ) ;
#64040=DIRECTION ( 'NONE',  ( 3.773278334444167608E-23, -1.000000000000000000, 0.000000000000000000 ) ) ;
#64041=CARTESIAN_POINT ( 'NONE',  ( -73.49934423242160619, -24.51314013834315375, 0.6176544820404108460 ) ) ;
#64044=CARTESIAN_POINT ( 'NONE',  ( -84.52287095715006160, -24.64898659630528854, 1.056161002820826145 ) ) ;
#64046=CARTESIAN_POINT ( 'NONE',  ( 11.02309159617336221, -17.05227643984133934, 11.49999999999998934 ) ) ;
#64047=B_SPLINE_CURVE_WITH_KNOTS ( 'NONE', 3,
 ( #46365, #40259, #46871, #79307, #39246, #70704 ),
 .UNSPECIFIED., .F., .F.,
 ( 4, 2, 4 ),
 ( 0.000000000000000000, 0.001380764517853250335, 0.002761529035706500670 ),
 .UNSPECIFIED. ) ;
#64048=DIRECTION ( 'NONE',  ( 0.000000000000000000, -0.9999999999976377785, -2.173523156925978705E-06 ) ) ;
#64049=FACE_OUTER_BOUND ( 'NONE', #44991, .T. ) ;
#64050=CARTESIAN_POINT ( 'NONE',  ( -59.51515945767989280, -23.73791477778911840, 11.05961554403171299 ) ) ;
#64051=EDGE_CURVE ( 'NONE', #5942, #19180, #52389, .T. ) ;
#64053=DIRECTION ( 'NONE',  ( -3.773278334453079618E-23, 0.9999999999976377785, 2.173523156925979975E-06 ) ) ;
#64054=CARTESIAN_POINT ( 'NONE',  ( -3.482456173223098528, 20.84670800329844198, 11.49999999999999645 ) ) ;
#64056=CARTESIAN_POINT ( 'NONE',  ( 14.67205787815721862, 16.58792043909384262, 11.49999999999998934 ) ) ;
#64057=EDGE_CURVE ( 'NONE', #27910, #64814, #89459, .T. ) ;
#64058=CARTESIAN_POINT ( 'NONE',  ( -20.17529555308526668, -4.016306826964139098, -1.500000000000002220 ) ) ;
#64060=CARTESIAN_POINT ( 'NONE',  ( -88.52287095715006160, -29.50250243563736774, 8.947779886222139822 ) ) ;
#64061=ORIENTED_EDGE ( 'NONE', *, *, #82964, .T. ) ;
#64062=CARTESIAN_POINT ( 'NONE',  ( -54.62799017530142009, -24.51314013834315020, 0.6176544820404069602 ) ) ;
#64063=LINE ( 'NONE', #94975, #8049 ) ;
#64065=VERTEX_POINT ( 'NONE', #29536 ) ;
#64067=CARTESIAN_POINT ( 'NONE',  ( -100.5228709571500900, -23.84047902841603417, -0.8780736468305739839 ) ) ;
#64070=CARTESIAN_POINT ( 'NONE',  ( -1.843323519027639357, -20.62917239659568835, -1.500000000000002220 ) ) ;
#64071=CARTESIAN_POINT ( 'NONE',  ( 19.51036611237648088, 9.378288983258578071, 11.49999999999999645 ) ) ;
#64074=CARTESIAN_POINT ( 'NONE',  ( -111.7766968413051671, -25.28171427076103583, 4.234743059359621142 ) ) ;
#64075=CARTESIAN_POINT ( 'NONE',  ( 22.22467975111640470, 2.813832150844377100, -1.500000000000002220 ) ) ;
#64076=CARTESIAN_POINT ( 'NONE',  ( -79.42863770186421846, -25.27874940277076732, 6.408999251374608797 ) ) ;
#64078=ORIENTED_EDGE ( 'NONE', *, *, #66061, .T. ) ;
#64080=CARTESIAN_POINT ( 'NONE',  ( -83.62287095715005592, -24.64898659630528854, 1.056161002820826145 ) ) ;
#64081=ORIENTED_EDGE ( 'NONE', *, *, #4372, .T. ) ;
#64084=CARTESIAN_POINT ( 'NONE',  ( -45.52287095715006160, -23.47596703998600631, 11.44779298504229104 ) ) ;
#64085=ORIENTED_EDGE ( 'NONE', *, *, #71779, .F. ) ;
#64086=DIRECTION ( 'NONE',  ( 0.000000000000000000, 2.173523156925980399E-06, -0.9999999999976378895 ) ) ;
#64087=CARTESIAN_POINT ( 'NONE',  ( 19.37530031839547107, -8.734557088507903799, -1.500000000000002220 ) ) ;
#64089=DIRECTION ( 'NONE',  ( 0.000000000000000000, -2.173523156925980399E-06, 0.9999999999976378895 ) ) ;
#64090=CARTESIAN_POINT ( 'NONE',  ( -17.41291239988371231, 13.16847401419012975, 11.49999999999998934 ) ) ;
#64091=CARTESIAN_POINT ( 'NONE',  ( -52.64485392522220053, -23.96169478059712787, 10.65365249895718591 ) ) ;
#64092=DIRECTION ( 'NONE',  ( 0.000000000000000000, 2.173523156925980399E-06, -0.9999999999976378895 ) ) ;
#64093=CARTESIAN_POINT ( 'NONE',  ( -116.6228709571500985, -23.73907113216991860, -1.053371485793224371 ) ) ;
#64094=CARTESIAN_POINT ( 'NONE',  ( 13.92123049006271707, -16.85212209846622855, -1.500000000000002220 ) ) ;
#64095=CARTESIAN_POINT ( 'NONE',  ( -30.57287095715006942, -24.05021112939445871, -0.4555005541943638048 ) ) ;
#64096=ORIENTED_EDGE ( 'NONE', *, *, #6213, .F. ) ;
#64098=CARTESIAN_POINT ( 'NONE',  ( -85.58560456462899424, -24.73531770709095312, 8.716586749053508498 ) ) ;
#64102=ORIENTED_EDGE ( 'NONE', *, *, #94165, .T. ) ;
#64103=VERTEX_POINT ( 'NONE', #99534 ) ;
#64105=CARTESIAN_POINT ( 'NONE',  ( -82.52213984707648819, -23.48783264082478439, -1.443836473390069486 ) ) ;
#64106=CARTESIAN_POINT ( 'NONE',  ( 15.87343765641381665, 14.11872912734625274, -1.500000000000002220 ) ) ;
#64107=LINE ( 'NONE', #41248, #10971 ) ;
#64108=DIRECTION ( 'NONE',  ( 0.000000000000000000, 2.173523156925980399E-06, -0.9999999999976378895 ) ) ;
#64110=CARTESIAN_POINT ( 'NONE',  ( -48.58953762381672448, -23.47596703998600276, 11.44779298504227505 ) ) ;
#64111=CARTESIAN_POINT ( 'NONE',  ( 8.513215801882951794, -17.43586836189350819, -1.500000000000002220 ) ) ;
#64112=CARTESIAN_POINT ( 'NONE',  ( -45.53132931798297989, -24.73486907724918282, 1.287355809206962576 ) ) ;
#64115=CARTESIAN_POINT ( 'NONE',  ( 0.2958748881272694198, 19.47992435465491212, 11.49999999999999645 ) ) ;
#64117=ADVANCED_FACE ( 'NONE', ( #22900 ), #6701, .F. ) ;
#64118=B_SPLINE_CURVE_WITH_KNOTS ( 'NONE', 3,
 ( #86765, #79150, #17253, #78632 ),
 .UNSPECIFIED., .F., .F.,
 ( 4, 4 ),
 ( 0.2889692275360895013, 0.2899699745768550274 ),
 .UNSPECIFIED. ) ;
#64120=ORIENTED_EDGE ( 'NONE', *, *, #30425, .T. ) ;
#64124=ADVANCED_FACE ( 'NONE', ( #54391 ), #50663, .T. ) ;
#64125=CARTESIAN_POINT ( 'NONE',  ( -111.5228709571500616, -24.64965694238407323, 8.947790433994192938 ) ) ;
#64126=CARTESIAN_POINT ( 'NONE',  ( -81.87824661256287584, -25.03155794964914094, 6.339755953538114497 ) ) ;
#64127=CARTESIAN_POINT ( 'NONE',  ( 13.10555085358618221, -14.64361678476065087, -1.500000000000002220 ) ) ;
#64128=ORIENTED_EDGE ( 'NONE', *, *, #78076, .T. ) ;
#64129=VECTOR ( 'NONE', #14816, 1000.000000000000114 ) ;
#64130=FACE_OUTER_BOUND ( 'NONE', #75601, .T. ) ;
#64131=CARTESIAN_POINT ( 'NONE',  ( -46.58953762381672448, -23.47593901973091235, -1.443836447539009749 ) ) ;
#64133=EDGE_CURVE ( 'NONE', #71901, #70309, #90714, .T. ) ;
#64138=CARTESIAN_POINT ( 'NONE',  ( -81.90174979306682701, -25.31249729222309597, 5.276660411446114196 ) ) ;
#64139=CARTESIAN_POINT ( 'NONE',  ( -43.62287095715007013, -24.35013146730203459, 9.818937971375111928 ) ) ;
#64140=B_SPLINE_CURVE_WITH_KNOTS ( 'NONE', 3,
 ( #37632, #22882, #99514, #91914, #74, #22389, #53373, #14785, #84298, #7684, #45750, #76671, #7177, #100006, #38126, #39131, #53870, #84802 ),
 .UNSPECIFIED., .F., .F.,
 ( 4, 2, 2, 2, 2, 2, 2, 2, 4 ),
 ( 0.004711262329854449225, 0.005300180574508829220, 0.005889098819163209216, 0.006478017063817618701, 0.007066935308472027319, 0.007655853553126437672, 0.008244771797780846290, 0.008833690042435254908, 0.009422608287089665260 ),
 .UNSPECIFIED. ) ;
#64141=CARTESIAN_POINT ( 'NONE',  ( -76.52287095715007581, -23.47596703998600631, 11.44779298504228571 ) ) ;
#64143=CARTESIAN_POINT ( 'NONE',  ( -13.68957358570155769, -14.46295258127404892, -1.500000000000002220 ) ) ;
#64144=CARTESIAN_POINT ( 'NONE',  ( -75.58253123086370806, -24.83644354573578994, 8.397322867130100121 ) ) ;
#64145=CARTESIAN_POINT ( 'NONE',  ( -1.214729172165279092, -19.82145330704504360, -1.500000000000002220 ) ) ;
#64146=ORIENTED_EDGE ( 'NONE', *, *, #90211, .F. ) ;
#64148=CARTESIAN_POINT ( 'NONE',  ( -125.5228709571500900, -24.91544648472620693, 1.928969306349231028 ) ) ;
#64149=DIRECTION ( 'NONE',  ( -3.773278334453079618E-23, 0.9999999999976377785, 2.173523156925979975E-06 ) ) ;
#64150=CARTESIAN_POINT ( 'NONE',  ( 9.628234360240019996, 18.42577530400075858, 11.49999999999999645 ) ) ;
#64151=CARTESIAN_POINT ( 'NONE',  ( -81.60465383657505356, -23.48783264082478084, -1.443836473390067043 ) ) ;
#64152=CARTESIAN_POINT ( 'NONE',  ( -106.5198659666137644, -23.73766607897671221, -1.055555164236449572 ) ) ;
#64153=CARTESIAN_POINT ( 'NONE',  ( -12.29745307268338195, -19.16510367807413218, 11.49999999999999645 ) ) ;
#64154=VECTOR ( 'NONE', #82622, 1000.000000000000114 ) ;
#64155=ORIENTED_EDGE ( 'NONE', *, *, #51906, .F. ) ;
#64156=CARTESIAN_POINT ( 'NONE',  ( -91.62287095715004170, -24.33832256527047733, 0.1851278514138617048 ) ) ;
#64159=ORIENTED_EDGE ( 'NONE', *, *, #27772, .F. ) ;
#64160=VECTOR ( 'NONE', #43886, 1000.000000000000114 ) ;
#64161=CARTESIAN_POINT ( 'NONE',  ( -20.01257119864951051, 2.908879540851186274, 11.49999999999998934 ) ) ;
#64162=CARTESIAN_POINT ( 'NONE',  ( -55.62287095715004881, -25.00158670708909625, 2.256160236439165967 ) ) ;
#64163=AXIS2_PLACEMENT_3D ( 'NONE', #13031, #36381, #44501 ) ;
#64164=CARTESIAN_POINT ( 'NONE',  ( -49.55620429048340014, -24.65952944569304606, 1.056160979905693909 ) ) ;
#64167=VERTEX_POINT ( 'NONE', #56909 ) ;
#64169=CARTESIAN_POINT ( 'NONE',  ( -84.52287095715004739, -24.50321055353805377, 9.387540953477524042 ) ) ;
#64170=CARTESIAN_POINT ( 'NONE',  ( -15.86121933104946535, 12.22609501325904624, -1.500000000000002220 ) ) ;
#64171=PLANE ( 'NONE',  #75556 ) ;
#64172=CARTESIAN_POINT ( 'NONE',  ( -8.441512789788195192, 19.21024974253229800, 11.49999999999999645 ) ) ;
#64173=CARTESIAN_POINT ( 'NONE',  ( -29.58433278696464797, -25.11104544706328667, 6.768552479589499349 ) ) ;
#64175=CARTESIAN_POINT ( 'NONE',  ( -8.753671783739276790, -20.25744411100385634, 11.49999999999998934 ) ) ;
#64176=ADVANCED_FACE ( 'NONE', ( #78203 ), #85832, .F. ) ;
#64178=VERTEX_POINT ( 'NONE', #9713 ) ;
#64179=CARTESIAN_POINT ( 'NONE',  ( -86.52287095715006160, -23.47593901973090169, -1.443836447538996648 ) ) ;
#64181=CARTESIAN_POINT ( 'NONE',  ( -72.53830702939148978, -24.65952944569304250, 1.056160979905695463 ) ) ;
#64182=EDGE_LOOP ( 'NONE', ( #49284, #54114, #80915, #66323 ) ) ;
#64186=LINE ( 'NONE', #17984, #82566 ) ;
#64187=CARTESIAN_POINT ( 'NONE',  ( -101.1996739087839075, -25.27404679889542294, 3.060140427661463214 ) ) ;
#64188=DIRECTION ( 'NONE',  ( 0.000000000000000000, 0.9999999999976377785, 2.173523156925979975E-06 ) ) ;
#64189=CARTESIAN_POINT ( 'NONE',  ( 8.954683214801249846, 18.48387022957959047, -1.500000000000002220 ) ) ;
#64190=ORIENTED_EDGE ( 'NONE', *, *, #99360, .F. ) ;
#64191=LINE ( 'NONE', #65195, #83404 ) ;
#64194=CARTESIAN_POINT ( 'NONE',  ( 3.885606641962014329, -21.97303888676646721, -1.500000000000002220 ) ) ;
#64195=CARTESIAN_POINT ( 'NONE',  ( -81.62287095715008434, -23.72747288104441665, -1.053458166803661555 ) ) ;
#64196=CARTESIAN_POINT ( 'NONE',  ( -26.35650876483003557, -24.67614927925039936, 7.701557122907957798 ) ) ;
#64197=ORIENTED_EDGE ( 'NONE', *, *, #37967, .F. ) ;
#64198=CARTESIAN_POINT ( 'NONE',  ( -50.52287095715007581, -25.00182538069144655, 7.747789668545104647 ) ) ;
#64201=CARTESIAN_POINT ( 'NONE',  ( -14.93763623016880082, -14.57113377498261997, -1.500000000000002220 ) ) ;
#64202=ORIENTED_EDGE ( 'NONE', *, *, #36699, .F. ) ;
#64203=CARTESIAN_POINT ( 'NONE',  ( -52.52287095715007581, -23.96127896942151025, -0.6493128930935695431 ) ) ;
#64205=VERTEX_POINT ( 'NONE', #48795 ) ;
#64206=CARTESIAN_POINT ( 'NONE',  ( -70.34543693012690824, -25.03149372849369669, 7.563174219444441349 ) ) ;
#64207=CARTESIAN_POINT ( 'NONE',  ( -1.165634184549018126, -21.02984315360824752, -1.500000000000002220 ) ) ;
#64209=CARTESIAN_POINT ( 'NONE',  ( -93.62287095715009855, -23.73934037231757799, 11.05740245334328975 ) ) ;
#64211=CARTESIAN_POINT ( 'NONE',  ( -105.6228709571500417, -29.50248789122583659, 2.256150453626215580 ) ) ;
#64212=CARTESIAN_POINT ( 'NONE',  ( -86.60313800047151744, -23.48786465467240703, 11.44779295918254647 ) ) ;
#64213=CARTESIAN_POINT ( 'NONE',  ( -59.64292777622080877, -23.96119346886879597, -0.6495511937832131322 ) ) ;
#64214=CARTESIAN_POINT ( 'NONE',  ( -14.64807036877012258, -15.96857234361563904, -1.500000000000002220 ) ) ;
#64216=CARTESIAN_POINT ( 'NONE',  ( -14.60993195340527251, 16.82711592829100411, 11.49999999999999645 ) ) ;
#64218=CARTESIAN_POINT ( 'NONE',  ( -51.48368152949297638, -25.31441875625928972, 5.903371675124650331 ) ) ;
#64219=CARTESIAN_POINT ( 'NONE',  ( -70.59960031398057367, -25.30103364020432011, 5.335303155633611460 ) ) ;
#64220=ORIENTED_EDGE ( 'NONE', *, *, #22599, .F. ) ;
#64224=ORIENTED_EDGE ( 'NONE', *, *, #97108, .F. ) ;
#64228=CARTESIAN_POINT ( 'NONE',  ( 19.96388892861992659, -2.714421270036905032, -1.500000000000002220 ) ) ;
#64229=CARTESIAN_POINT ( 'NONE',  ( -126.5228709571500616, -23.72773821059536914, 11.05748984161097326 ) ) ;
#64232=EDGE_CURVE ( 'NONE', #3436, #25180, #48305, .T. ) ;
#64233=CARTESIAN_POINT ( 'NONE',  ( -130.5728709571500588, -24.61658504062384978, 9.350733115928049344 ) ) ;
#64234=CARTESIAN_POINT ( 'NONE',  ( -21.67104271438225638, 5.786422744429515319, -1.500000000000002220 ) ) ;
#64236=EDGE_LOOP ( 'NONE', ( #17391, #93559, #58062, #88382 ) ) ;
#64238=CARTESIAN_POINT ( 'NONE',  ( -112.5139873076401074, -24.66019654487200086, 8.947790411086112172 ) ) ;
#64239=CARTESIAN_POINT ( 'NONE',  ( -101.5528284347318930, -24.15620529776628800, 10.23563542870660292 ) ) ;
#64241=CARTESIAN_POINT ( 'NONE',  ( -40.41683116089613748, -25.31532428806244539, 5.082404371757057504 ) ) ;
#64244=EDGE_CURVE ( 'NONE', #60701, #53473, #3571, .T. ) ;
#64245=CARTESIAN_POINT ( 'NONE',  ( -130.5728709571501440, -25.14064729901805961, 2.712351064733618422 ) ) ;
#64246=CARTESIAN_POINT ( 'NONE',  ( -18.05301863641116000, -7.546005365994440162, 11.49999999999998934 ) ) ;
#64248=CARTESIAN_POINT ( 'NONE',  ( -46.64014652896692326, -24.15543982623906416, -0.2315651400026683127 ) ) ;
#64250=CARTESIAN_POINT ( 'NONE',  ( -17.63906703526961550, 12.34593017946836291, 11.49999999999998934 ) ) ;
#64251=DIRECTION ( 'NONE',  ( -3.773278334453079618E-23, 0.9999999999976377785, 2.173523156925979975E-06 ) ) ;
#64252=EDGE_CURVE ( 'NONE', #62581, #31857, #56410, .T. ) ;
#64254=CARTESIAN_POINT ( 'NONE',  ( -53.62287095715005592, -23.47596703998600276, 11.44779298504227683 ) ) ;
#64256=CARTESIAN_POINT ( 'NONE',  ( -20.69623851537618364, -9.862649113751288610, -1.500000000000002220 ) ) ;
#64259=CARTESIAN_POINT ( 'NONE',  ( -71.30457154551150722, -25.25559839591754496, 6.209207386190694677 ) ) ;
#64260=CARTESIAN_POINT ( 'NONE',  ( -19.81368827760683260, -3.497637702615509880, 11.49999999999999645 ) ) ;
#64261=CARTESIAN_POINT ( 'NONE',  ( -110.1676456071266870, -25.28814069637450146, 2.835829433892736340 ) ) ;
#64265=EDGE_CURVE ( 'NONE', #2529, #55213, #74889, .T. ) ;
#64266=CARTESIAN_POINT ( 'NONE',  ( -53.52287095715008292, -23.47593901973090169, -1.443836447538997092 ) ) ;
#64267=CARTESIAN_POINT ( 'NONE',  ( 12.34629653512297409, 15.52844579862587437, -1.500000000000002220 ) ) ;
#64269=CARTESIAN_POINT ( 'NONE',  ( 0.7808950796103379943, -19.64173473864696717, -1.500000000000002220 ) ) ;
#64270=AXIS2_PLACEMENT_3D ( 'NONE', #32413, #71989, #93295 ) ;
#64271=CARTESIAN_POINT ( 'NONE',  ( -42.49914285597344588, -24.15543982623907127, -0.2315651400026575435 ) ) ;
#64272=CARTESIAN_POINT ( 'NONE',  ( -71.58953762381672448, -23.47593901973091235, -1.443836447539006196 ) ) ;
#64274=CARTESIAN_POINT ( 'NONE',  ( -60.52287095715006160, -24.91570333826269490, 8.075032458230454679 ) ) ;
#64275=CARTESIAN_POINT ( 'NONE',  ( -39.04717358288242934, -25.28743336242031958, 4.335731970569660199 ) ) ;
#64276=CARTESIAN_POINT ( 'NONE',  ( -16.38011734009650411, 12.53836025512309149, 11.49999999999999645 ) ) ;
#64278=DIRECTION ( 'NONE',  ( -3.773278334453079618E-23, 0.9999999999976377785, 2.173523156925979975E-06 ) ) ;
#64279=CARTESIAN_POINT ( 'NONE',  ( -8.190886813464794969, 21.05079722441571732, 11.49999999999999645 ) ) ;
#64281=CARTESIAN_POINT ( 'NONE',  ( -69.41396772704672458, -25.12219025450763255, 6.552775786966387628 ) ) ;
#64283=CARTESIAN_POINT ( 'NONE',  ( -97.50711219967668342, -24.65952944569304606, 1.056160979905701680 ) ) ;
#64284=CARTESIAN_POINT ( 'NONE',  ( -126.5228709571500616, -23.47593901973090524, -1.443836447538996204 ) ) ;
#64286=CARTESIAN_POINT ( 'NONE',  ( -27.70544111104076990, -24.61460113826161944, 8.251826784989919616 ) ) ;
#64287=DIRECTION ( 'NONE',  ( 1.000000000000000000, 3.773278334444166432E-23, 8.201307841325785021E-29 ) ) ;
#64289=ADVANCED_FACE ( 'NONE', ( #27936 ), #65033, .F. ) ;
#64290=ORIENTED_EDGE ( 'NONE', *, *, #78866, .F. ) ;
#64291=CARTESIAN_POINT ( 'NONE',  ( 22.28998074345494729, -6.091270044117925053, 11.49999999999999645 ) ) ;
#64292=CARTESIAN_POINT ( 'NONE',  ( -21.74551633039419585, 6.958787177381512201, -1.500000000000002220 ) ) ;
#64293=CARTESIAN_POINT ( 'NONE',  ( -100.4326965455115044, -25.18492896333868103, 3.293943116708551777 ) ) ;
#64294=CARTESIAN_POINT ( 'NONE',  ( -115.5228709571500190, -24.62285846331437966, 9.038163153548229189 ) ) ;
#64295=CARTESIAN_POINT ( 'NONE',  ( -82.59550797413433543, -23.96169478059713143, 10.65365249895718414 ) ) ;
#64296=CARTESIAN_POINT ( 'NONE',  ( 20.54305097139451064, 9.177977666691313985, 11.49999999999999645 ) ) ;
#64297=ORIENTED_EDGE ( 'NONE', *, *, #3918, .F. ) ;
#64298=CARTESIAN_POINT ( 'NONE',  ( -43.58705352746476791, -24.34968618360933590, 0.1864209137778851388 ) ) ;
#64299=CARTESIAN_POINT ( 'NONE',  ( 10.99670386783381737, -19.00842362925918749, -1.500000000000002220 ) ) ;
#64300=CARTESIAN_POINT ( 'NONE',  ( -81.62287095715005592, -29.50250243563736774, 8.947779886222141599 ) ) ;
#64301=CARTESIAN_POINT ( 'NONE',  ( -34.57521954910300366, -24.66019654487199730, 8.947790411086117501 ) ) ;
#64302=CARTESIAN_POINT ( 'NONE',  ( -69.63426884387564542, -25.06829995203217720, 7.393698517222913935 ) ) ;
#64306=PLANE ( 'NONE',  #13786 ) ;
#64307=ORIENTED_EDGE ( 'NONE', *, *, #44864, .F. ) ;
#64309=CARTESIAN_POINT ( 'NONE',  ( -19.72667040167412722, -5.651925516699977337, 11.49999999999998934 ) ) ;
#64310=ORIENTED_EDGE ( 'NONE', *, *, #98670, .T. ) ;
#64312=ORIENTED_EDGE ( 'NONE', *, *, #89211, .T. ) ;
#64314=B_SPLINE_CURVE_WITH_KNOTS ( 'NONE', 3,
 ( #20114, #42972, #73908, #82019 ),
 .UNSPECIFIED., .F., .F.,
 ( 4, 4 ),
 ( 0.000000000000000000, 9.999999999998897304E-05 ),
 .UNSPECIFIED. ) ;
#64316=CARTESIAN_POINT ( 'NONE',  ( -50.37830952628071657, -25.31401921878212136, 5.197788989978542773 ) ) ;
#64317=CARTESIAN_POINT ( 'NONE',  ( 1.767912858038628965, -23.04938964843747584, -1.500000000000002220 ) ) ;
#64318=CARTESIAN_POINT ( 'NONE',  ( -116.6228709571500559, -29.50250786944525672, 11.44777988621622811 ) ) ;
#64319=CARTESIAN_POINT ( 'NONE',  ( 6.737473828552405841, -19.20966278261563076, -1.500000000000002220 ) ) ;
#64321=ORIENTED_EDGE ( 'NONE', *, *, #84929, .F. ) ;
#64323=CARTESIAN_POINT ( 'NONE',  ( -29.63599055435521024, -24.27518589826293649, 9.817618405055078767 ) ) ;
#64325=CARTESIAN_POINT ( 'NONE',  ( -114.6228709571500701, -23.73934037231757799, 11.05740245334328442 ) ) ;
#64327=CARTESIAN_POINT ( 'NONE',  ( -10.32266838563235467, 18.89866041204108527, 11.49999999999999645 ) ) ;
#64329=CARTESIAN_POINT ( 'NONE',  ( -29.24616400714660003, -25.21532219221842652, 4.855716927727858234 ) ) ;
#64332=CARTESIAN_POINT ( 'NONE',  ( -20.73834036848188234, 1.213307192923735345, 11.49999999999998934 ) ) ;
#64335=CARTESIAN_POINT ( 'NONE',  ( -125.6241961315440534, -24.63355581998386512, 0.9682620441944075340 ) ) ;
#64336=ORIENTED_EDGE ( 'NONE', *, *, #45124, .F. ) ;
#64337=CARTESIAN_POINT ( 'NONE',  ( -47.62287095715004881, -23.48783264082478084, -1.443836473390070596 ) ) ;
#64342=CARTESIAN_POINT ( 'NONE',  ( -129.5228709571500758, -29.50248528299804818, 1.056150453629047137 ) ) ;
#64343=CARTESIAN_POINT ( 'NONE',  ( -78.52287095715001897, -24.33832256527049154, 0.1851278514138635367 ) ) ;
#64344=CARTESIAN_POINT ( 'NONE',  ( 21.30657626330824783, 5.479626006175059239, 11.49999999999999645 ) ) ;
#64346=CARTESIAN_POINT ( 'NONE',  ( -103.5530519847491178, -24.15543982623907482, -0.2315651400026619011 ) ) ;
#64347=CARTESIAN_POINT ( 'NONE',  ( 10.27952223434480494, 20.12118371629609470, -1.500000000000002220 ) ) ;
#64350=ORIENTED_EDGE ( 'NONE', *, *, #7060, .T. ) ;
#64351=VERTEX_POINT ( 'NONE', #34557 ) ;
#64353=CARTESIAN_POINT ( 'NONE',  ( -88.52287095715006160, -23.48786465467241769, 11.44779295918254292 ) ) ;
#64354=B_SPLINE_CURVE_WITH_KNOTS ( 'NONE', 3,
 ( #83006, #50091, #20121, #66324, #12507, #43472, #34856, #13496, #97744, #72925, #74411, #4904, #35850, #3426, #34359, #96257 ),
 .UNSPECIFIED., .F., .F.,
 ( 4, 2, 2, 2, 2, 2, 2, 4 ),
 ( 0.000000000000000000, 0.0001832628685938118200, 0.0003665257371876236400, 0.0005497886057814354872, 0.0007330514743752472801, 0.001099577211562870974, 0.001282840080156677455, 0.001466102948750484152 ),
 .UNSPECIFIED. ) ;
#64355=CARTESIAN_POINT ( 'NONE',  ( -36.58953762381673158, -24.64965694238406613, 8.947790433994660120 ) ) ;
#64356=ORIENTED_EDGE ( 'NONE', *, *, #67108, .F. ) ;
#64357=CARTESIAN_POINT ( 'NONE',  ( -17.86006801910157193, 11.38285951858322242, 11.49999999999998934 ) ) ;
#64361=DIRECTION ( 'NONE',  ( 3.773278334444167608E-23, -1.000000000000000000, 0.000000000000000000 ) ) ;
#64362=CARTESIAN_POINT ( 'NONE',  ( 21.18294168759468832, 6.642818831845659133, -1.500000000000002220 ) ) ;
#64363=CARTESIAN_POINT ( 'NONE',  ( -114.5882204601105059, -24.51314013834316086, 0.6176544820404237246 ) ) ;
#64366=CARTESIAN_POINT ( 'NONE',  ( -79.92287095715005307, -23.47596703998600631, 11.44779298504227860 ) ) ;
#64368=CARTESIAN_POINT ( 'NONE',  ( -12.45040968399260883, -14.89389333286084671, 11.49999999999999645 ) ) ;
#64370=CARTESIAN_POINT ( 'NONE',  ( -41.15367109091464215, -25.13982731016471917, 3.000623932295935159 ) ) ;
#64372=CARTESIAN_POINT ( 'NONE',  ( 17.91360334016800593, 7.682165803940314674, -1.500000000000002220 ) ) ;
#64374=CARTESIAN_POINT ( 'NONE',  ( 13.27131465344908001, -16.79725507166503462, -1.500000000000002220 ) ) ;
#64375=CARTESIAN_POINT ( 'NONE',  ( -32.55620429048337172, -24.64965694238574301, 8.947790433994212478 ) ) ;
#64376=CARTESIAN_POINT ( 'NONE',  ( -60.50379446447523435, -24.15602025861357660, 10.28564288302606933 ) ) ;
#64378=LINE ( 'NONE', #17167, #66543 ) ;
#64379=DIRECTION ( 'NONE',  ( -3.773278334453079618E-23, 0.9999999999976377785, 2.173523156925979975E-06 ) ) ;
#64380=CARTESIAN_POINT ( 'NONE',  ( -13.93578158028743985, 17.96481793202167054, -1.500000000000002220 ) ) ;
#64381=AXIS2_PLACEMENT_3D ( 'NONE', #90839, #5102, #99438 ) ;
#64384=CARTESIAN_POINT ( 'NONE',  ( -106.6264150236442134, -24.35071581493544457, 9.817618358456019934 ) ) ;
#64386=CARTESIAN_POINT ( 'NONE',  ( -19.77041435686880533, -2.435487021107205940, 11.49999999999999645 ) ) ;
#64390=CARTESIAN_POINT ( 'NONE',  ( -51.22287095715007155, -23.47593901973090169, -1.443836447538997758 ) ) ;
#64393=CARTESIAN_POINT ( 'NONE',  ( -49.58084058178877029, -25.16964401093727943, 6.816005909056730871 ) ) ;
#64394=CARTESIAN_POINT ( 'NONE',  ( -31.80980768408297266, -25.31600595412499644, 6.101236642668423471 ) ) ;
#64395=CARTESIAN_POINT ( 'NONE',  ( -117.6228709571500701, -24.66019654487199730, 8.947790411086121054 ) ) ;
#64396=CARTESIAN_POINT ( 'NONE',  ( -7.614213781628100364, -20.28429660096114517, 11.49999999999998934 ) ) ;
#64398=CARTESIAN_POINT ( 'NONE',  ( 18.23270504744370868, -6.907985942191454676, -1.500000000000002220 ) ) ;
#64399=CARTESIAN_POINT ( 'NONE',  ( -67.62287095715008434, -23.47596703998600276, 11.44779298504227505 ) ) ;
#64400=VERTEX_POINT ( 'NONE', #80730 ) ;
#64401=PLANE ( 'NONE',  #88893 ) ;
#64402=CARTESIAN_POINT ( 'NONE',  ( -19.36681041099238598, 6.328833669845586485, 11.49999999999999645 ) ) ;
#64404=CARTESIAN_POINT ( 'NONE',  ( -60.91704397828815587, -25.27796947198809363, 6.054720049563738549 ) ) ;
#64406=CARTESIAN_POINT ( 'NONE',  ( -41.46611000704998418, -25.28830591450888932, 4.188173661249235735 ) ) ;
#64408=CARTESIAN_POINT ( 'NONE',  ( -49.22287095715006444, -23.47596703998600276, 11.44779298504227683 ) ) ;
#64409=CARTESIAN_POINT ( 'NONE',  ( -49.27764846858840997, -25.25138878606429671, 6.145204991494091828 ) ) ;
#64411=CARTESIAN_POINT ( 'NONE',  ( -109.5877490058777539, -24.51314013834315730, 0.6176544820404190617 ) ) ;
#64413=CARTESIAN_POINT ( 'NONE',  ( -66.54009212403214235, -24.51419770103157347, 9.386484678747176957 ) ) ;
#64416=CARTESIAN_POINT ( 'NONE',  ( 19.50756536182865020, -12.10693203178887423, 11.49999999999999645 ) ) ;
#64417=CARTESIAN_POINT ( 'NONE',  ( 0.6941480231959694658, 22.73124288027050710, -1.500000000000002220 ) ) ;
#64421=CARTESIAN_POINT ( 'NONE',  ( -90.58192396404253088, -25.00158670708910691, 2.256160236439220590 ) ) ;
#64423=CARTESIAN_POINT ( 'NONE',  ( -69.55365840088312268, -25.18627906957131657, 6.773493112845361708 ) ) ;
#64424=CARTESIAN_POINT ( 'NONE',  ( -18.33957545910867282, 11.93505917737106259, 11.49999999999998934 ) ) ;
#64425=CARTESIAN_POINT ( 'NONE',  ( -70.52287095715007581, -24.99132157543166599, 2.256160258750667502 ) ) ;
#64428=CARTESIAN_POINT ( 'NONE',  ( -122.5885215633497296, -24.65952944569305316, 1.056160979905708786 ) ) ;
#64432=CARTESIAN_POINT ( 'NONE',  ( -15.55180764702766716, 13.24544322234432414, -1.500000000000002220 ) ) ;
#64433=VERTEX_POINT ( 'NONE', #19808 ) ;
#64435=CARTESIAN_POINT ( 'NONE',  ( 22.64363655503811046, -4.068770074275382953, 11.49999999999998934 ) ) ;
#64436=DIRECTION ( 'NONE',  ( -1.000000000000000000, -3.773278334444167608E-23, -8.201307833595939069E-29 ) ) ;
#64437=B_SPLINE_CURVE_WITH_KNOTS ( 'NONE', 3,
 ( #25540, #65129, #42295, #73223, #3713, #58009 ),
 .UNSPECIFIED., .F., .F.,
 ( 4, 2, 4 ),
 ( 0.000000000000000000, 0.001380764517854765399, 0.002761529035709530799 ),
 .UNSPECIFIED. ) ;
#64439=CARTESIAN_POINT ( 'NONE',  ( -94.52287095715006160, -29.50248528299804818, 1.056150453629040253 ) ) ;
#64440=VECTOR ( 'NONE', #49502, 1000.000000000000114 ) ;
#64441=CARTESIAN_POINT ( 'NONE',  ( -32.55620429048339304, -24.65952944569304606, 1.056160979905692132 ) ) ;
#64442=CARTESIAN_POINT ( 'NONE',  ( -98.62287095715005592, -23.48786465467241769, 11.44779295918254292 ) ) ;
#64444=CARTESIAN_POINT ( 'NONE',  ( 15.78869406909177897, -14.30566568001193950, 11.49999999999999645 ) ) ;
#64446=EDGE_LOOP ( 'NONE', ( #58439, #4051, #41293, #90878 ) ) ;
#64447=CARTESIAN_POINT ( 'NONE',  ( 12.24756355222007898, 18.56953561607567238, 11.49999999999998934 ) ) ;
#64448=CARTESIAN_POINT ( 'NONE',  ( 20.52162115075873672, 2.272738508513782119, 11.49999999999998934 ) ) ;
#64455=CARTESIAN_POINT ( 'NONE',  ( -65.62287095715005592, -25.00158670708909270, 2.256160236439166855 ) ) ;
#64459=CARTESIAN_POINT ( 'NONE',  ( -71.30457154551152144, -25.24554880456021522, 6.209207408033732278 ) ) ;
#64460=CARTESIAN_POINT ( 'NONE',  ( 12.78316523911058944, -16.47895720935621711, -1.500000000000002220 ) ) ;
#64461=CARTESIAN_POINT ( 'NONE',  ( -15.20188179817220231, 15.67080601223297442, 11.49999999999999645 ) ) ;
#64462=CARTESIAN_POINT ( 'NONE',  ( -73.58796373308013017, -24.35071581493543036, 9.817618358456027039 ) ) ;
#64463=CARTESIAN_POINT ( 'NONE',  ( -75.62287095715005592, -29.50247984919015209, -1.443849546365053582 ) ) ;
#64464=CARTESIAN_POINT ( 'NONE',  ( -20.52357230491503159, 9.176553703681571861, -1.500000000000002220 ) ) ;
#64466=EDGE_CURVE ( 'NONE', #21027, #3669, #19179, .T. ) ;
#64467=CARTESIAN_POINT ( 'NONE',  ( -8.531171415479239073, -19.09552649099111221, -1.500000000000002220 ) ) ;
#64468=CARTESIAN_POINT ( 'NONE',  ( -26.15327376889522526, -24.97066975962406943, 5.797585818533663726 ) ) ;
#64472=ORIENTED_EDGE ( 'NONE', *, *, #63936, .T. ) ;
#64475=ORIENTED_EDGE ( 'NONE', *, *, #35936, .T. ) ;
#64476=CARTESIAN_POINT ( 'NONE',  ( 21.30238844577196389, 2.035401582669650544, -1.500000000000002220 ) ) ;
#64477=CARTESIAN_POINT ( 'NONE',  ( -20.28323820415832657, -9.445149539555593776, 11.49999999999999645 ) ) ;
#64478=EDGE_LOOP ( 'NONE', ( #30926, #11013, #32637, #53065 ) ) ;
#64479=CARTESIAN_POINT ( 'NONE',  ( -28.55620429048338949, -23.31442300727656658, 11.44779301120574999 ) ) ;
#64480=CARTESIAN_POINT ( 'NONE',  ( 8.294003578737715543, -19.35633765900385939, 11.49999999999998934 ) ) ;
#64481=CARTESIAN_POINT ( 'NONE',  ( -30.51821509024741275, -25.31107878299565783, 5.002391647799127483 ) ) ;
#64482=CARTESIAN_POINT ( 'NONE',  ( 10.08953278062578462, 17.19620541797624824, -1.500000000000002220 ) ) ;
#64484=CARTESIAN_POINT ( 'NONE',  ( -122.6228709571500417, -23.47596703998600631, 11.44779298504227860 ) ) ;
#64485=CARTESIAN_POINT ( 'NONE',  ( -21.82725030464235516, 2.967780500094957308, -1.500000000000002220 ) ) ;
#64486=ORIENTED_EDGE ( 'NONE', *, *, #21717, .T. ) ;
#64487=CARTESIAN_POINT ( 'NONE',  ( -116.5914121302601387, -23.96119346886881729, -0.6495511937831833782 ) ) ;
#64488=EDGE_CURVE ( 'NONE', #26504, #26877, #19315, .T. ) ;
#64489=LINE ( 'NONE', #79170, #15721 ) ;
#64490=CARTESIAN_POINT ( 'NONE',  ( -40.76794460738368997, -25.31624736906593043, 5.521532656993860755 ) ) ;
#64491=AXIS2_PLACEMENT_3D ( 'NONE', #74053, #36480, #51216 ) ;
#64492=CARTESIAN_POINT ( 'NONE',  ( -62.59791734348949177, -23.96169478059712432, 10.65365249895718414 ) ) ;
#64494=CARTESIAN_POINT ( 'NONE',  ( -48.58953762381673158, -23.47593901973091235, -1.443836447539009749 ) ) ;
#64495=CARTESIAN_POINT ( 'NONE',  ( -4.607724273132460802, 20.83226218841027944, -1.500000000000002220 ) ) ;
#64496=FACE_OUTER_BOUND ( 'NONE', #40452, .T. ) ;
#64497=LINE ( 'NONE', #24890, #38182 ) ;
#64498=EDGE_CURVE ( 'NONE', #85110, #6180, #85678, .T. ) ;
#64501=CARTESIAN_POINT ( 'NONE',  ( 2.010693963185784749, 22.50221635003889276, -1.500000000000002220 ) ) ;
#64502=B_SPLINE_SURFACE_WITH_KNOTS ( 'NONE', 3, 3, ( 
 ( #98037, #20408, #74704, #28050 ),
 ( #4213, #13300, #13799, #6198 ),
 ( #90935, #68112, #99032, #21407 ),
 ( #89941, #12801, #35167, #5202 ),
 ( #52383, #19429, #50394, #73718 ),
 ( #97053, #27556, #58510, #89447 ),
 ( #50892, #28533, #81831, #12303 ) ),
 .UNSPECIFIED., .F., .F., .F.,
 ( 4, 3, 4 ),
 ( 4, 4 ),
 ( 0.0004766839783823902305, 0.1029713700210900945, 0.2054660560637978084 ),
 ( 0.1195244022139620860, 0.1205922751095607898 ),
 .UNSPECIFIED. ) ;
#64506=DIRECTION ( 'NONE',  ( -3.773278334453079030E-23, 0.9999999999976377785, 2.173523156925979128E-06 ) ) ;
#64507=CARTESIAN_POINT ( 'NONE',  ( -122.6228709571500417, -24.50216790748098461, 0.6166512839513762501 ) ) ;
#64508=CARTESIAN_POINT ( 'NONE',  ( -15.16444148636751521, -12.51942901160708921, 11.49999999999999645 ) ) ;
#64510=CARTESIAN_POINT ( 'NONE',  ( -73.52287095715011844, -23.95044443724992789, 10.65354141964649415 ) ) ;
#64512=EDGE_CURVE ( 'NONE', #55708, #90958, #36539, .T. ) ;
#64513=CARTESIAN_POINT ( 'NONE',  ( -79.62632635320380814, -25.21083105912962097, 3.409327675794635581 ) ) ;
#64514=DIRECTION ( 'NONE',  ( -3.773278334453079030E-23, 0.9999999999976377785, 2.173523156925979128E-06 ) ) ;
#64516=DIRECTION ( 'NONE',  ( 0.000000000000000000, 0.9999999999976377785, 2.173523156925979975E-06 ) ) ;
#64517=AXIS2_PLACEMENT_3D ( 'NONE', #23520, #24033, #15919 ) ;
#64518=CARTESIAN_POINT ( 'NONE',  ( -120.5562042904834072, -24.99132157543166954, 2.256160258750667946 ) ) ;
#64519=EDGE_CURVE ( 'NONE', #41620, #29468, #1037, .T. ) ;
#64521=CARTESIAN_POINT ( 'NONE',  ( -17.60924879254659459, 8.996216891746938060, 11.49999999999998934 ) ) ;
#64522=VERTEX_POINT ( 'NONE', #37546 ) ;
#64523=CARTESIAN_POINT ( 'NONE',  ( 8.007726535620864894, 18.53121347637897287, 11.49999999999999645 ) ) ;
#64526=ORIENTED_EDGE ( 'NONE', *, *, #23411, .F. ) ;
#64528=CARTESIAN_POINT ( 'NONE',  ( -80.85529437621991633, -25.30559667752245900, 5.016674165721909162 ) ) ;
#64530=DIRECTION ( 'NONE',  ( -0.000000000000000000, 2.173523156925979552E-06, -0.9999999999976378895 ) ) ;
#64531=AXIS2_PLACEMENT_3D ( 'NONE', #29997, #1066, #53356 ) ;
#64532=CARTESIAN_POINT ( 'NONE',  ( -39.62287095715007723, -24.34917612406837861, 0.1852690917426592920 ) ) ;
#64533=B_SPLINE_CURVE_WITH_KNOTS ( 'NONE', 3,
 ( #8590, #9084, #39539, #48673, #63398, #40037 ),
 .UNSPECIFIED., .F., .F.,
 ( 4, 2, 4 ),
 ( 1.571618716487580835E-05, 0.001396934050510501013, 0.002778151913856126160 ),
 .UNSPECIFIED. ) ;
#64535=CARTESIAN_POINT ( 'NONE',  ( -11.57650325489309395, -16.32560983125179277, -1.500000000000002220 ) ) ;
#64536=CARTESIAN_POINT ( 'NONE',  ( -99.16315266720698673, -25.10935227823729576, 3.707282584693533778 ) ) ;
#64539=CARTESIAN_POINT ( 'NONE',  ( -103.5228709571500190, -23.73934037231756733, 11.05740245334328087 ) ) ;
#64542=DIRECTION ( 'NONE',  ( 0.000000000000000000, 0.9999999999976377785, 2.173523156925979975E-06 ) ) ;
#64544=CARTESIAN_POINT ( 'NONE',  ( -45.55620429048337883, -23.47596703998600276, 11.44779298504227505 ) ) ;
#64545=CARTESIAN_POINT ( 'NONE',  ( -101.9705984573116666, -25.11539320716599732, 2.804431449967498491 ) ) ;
#64546=ORIENTED_EDGE ( 'NONE', *, *, #55981, .T. ) ;
#64547=CARTESIAN_POINT ( 'NONE',  ( -20.32193514540556123, 0.06534614623005505218, -1.500000000000002220 ) ) ;
#64550=CARTESIAN_POINT ( 'NONE',  ( -127.6242802972114276, -23.96169478059713853, 10.65365249895716637 ) ) ;
#64551=ORIENTED_EDGE ( 'NONE', *, *, #51502, .T. ) ;
#64553=CARTESIAN_POINT ( 'NONE',  ( -49.94169464672810221, -25.12215404331965019, 7.031228054708656749 ) ) ;
#64554=CARTESIAN_POINT ( 'NONE',  ( -30.47287095715006799, -25.22866023116455381, 3.592313111342048337 ) ) ;
#64555=CARTESIAN_POINT ( 'NONE',  ( 21.14167878903947084, -0.5806874866175276706, 11.49999999999999645 ) ) ;
#64556=CARTESIAN_POINT ( 'NONE',  ( 21.55033589006239936, 5.121329677682045833, 11.49999999999998934 ) ) ;
#64557=CARTESIAN_POINT ( 'NONE',  ( -1.452656003914881477, -20.50939586048694352, -1.500000000000002220 ) ) ;
#64558=ADVANCED_FACE ( 'NONE', ( #14696 ), #28929, .F. ) ;
#64560=CARTESIAN_POINT ( 'NONE',  ( -113.6228709571500417, -23.47596703998600631, 11.44779298504227860 ) ) ;
#64561=ORIENTED_EDGE ( 'NONE', *, *, #92157, .F. ) ;
#64562=CARTESIAN_POINT ( 'NONE',  ( -54.60549243945573039, -23.73766607897669445, -1.055555164236461563 ) ) ;
#64563=DIRECTION ( 'NONE',  ( -3.773278334444166432E-23, 1.000000000000000000, 0.000000000000000000 ) ) ;
#64564=ORIENTED_EDGE ( 'NONE', *, *, #55584, .F. ) ;
#64565=ORIENTED_EDGE ( 'NONE', *, *, #6793, .F. ) ;
#64566=ORIENTED_EDGE ( 'NONE', *, *, #18721, .F. ) ;
#64567=CARTESIAN_POINT ( 'NONE',  ( -103.5562042904834072, -23.48786465467241413, 11.44779295918253759 ) ) ;
#64568=CARTESIAN_POINT ( 'NONE',  ( -29.22287093065927976, -23.36589167027821290, -1.443836447538997314 ) ) ;
#64569=LINE ( 'NONE', #56446, #48780 ) ;
#64570=CARTESIAN_POINT ( 'NONE',  ( -16.63904852704994042, -12.34428335884295969, -1.500000000000002220 ) ) ;
#64571=B_SPLINE_CURVE_WITH_KNOTS ( 'NONE', 3,
 ( #92323, #46163, #15703, #85720, #46667, #39042 ),
 .UNSPECIFIED., .F., .F.,
 ( 4, 2, 4 ),
 ( 1.570887131794176733E-05, 0.001396322306279758037, 0.002776935741241574537 ),
 .UNSPECIFIED. ) ;
#64572=CARTESIAN_POINT ( 'NONE',  ( 21.64940796807912449, -0.2623997510114038922, 11.49999999999999645 ) ) ;
#64576=CARTESIAN_POINT ( 'NONE',  ( -111.4314572179059866, -25.19203390433109746, 3.343237222027082289 ) ) ;
#64577=CARTESIAN_POINT ( 'NONE',  ( 16.55124408090292576, 15.08944307983326638, -1.500000000000002220 ) ) ;
#64578=EDGE_CURVE ( 'NONE', #41986, #26092, #24024, .T. ) ;
#64580=B_SPLINE_CURVE_WITH_KNOTS ( 'NONE', 3,
 ( #68045, #28966, #24237, #16618, #93244, #23731, #79018, #17123 ),
 .UNSPECIFIED., .F., .F.,
 ( 4, 2, 2, 4 ),
 ( 0.000000000000000000, 0.002001079623178221058, 0.003001619434767333321, 0.004002159246356445585 ),
 .UNSPECIFIED. ) ;
#64581=EDGE_CURVE ( 'NONE', #45200, #30457, #6954, .T. ) ;
#64583=CARTESIAN_POINT ( 'NONE',  ( -61.62287095715004881, -24.64965695001468404, 8.947790433994185832 ) ) ;
#64588=VERTEX_POINT ( 'NONE', #38040 ) ;
#64590=CARTESIAN_POINT ( 'NONE',  ( -46.63379005058555293, -24.35071581493542325, 9.817618358456032368 ) ) ;
#64591=ORIENTED_EDGE ( 'NONE', *, *, #2709, .F. ) ;
#64593=CARTESIAN_POINT ( 'NONE',  ( 3.248270302591931724, 20.98854991013365279, -1.500000000000002220 ) ) ;
#64596=CARTESIAN_POINT ( 'NONE',  ( -12.45635911906152771, -17.91357634596933934, -1.500000000000002220 ) ) ;
#64597=CARTESIAN_POINT ( 'NONE',  ( -103.5151580449021509, -24.15620529776628445, 10.23563542870660292 ) ) ;
#64598=VECTOR ( 'NONE', #51394, 1000.000000000000114 ) ;
#64599=LINE ( 'NONE', #3184, #9655 ) ;
#64601=CARTESIAN_POINT ( 'NONE',  ( 3.414333255021221092, 21.62243999391013105, -1.500000000000002220 ) ) ;
#64605=CARTESIAN_POINT ( 'NONE',  ( -85.56477010883600087, -23.48786465467240703, 11.44779295918254647 ) ) ;
#64607=VERTEX_POINT ( 'NONE', #68992 ) ;
#64613=CARTESIAN_POINT ( 'NONE',  ( -82.59188034808971679, -24.15543982623907482, -0.2315651400026497997 ) ) ;
#64614=CARTESIAN_POINT ( 'NONE',  ( 21.10678091372558640, -2.468637549841573797, 11.49999999999998934 ) ) ;
#64615=DIRECTION ( 'NONE',  ( -3.773278334453080206E-23, 0.9999999999976377785, 2.173523156925979975E-06 ) ) ;
#64616=CARTESIAN_POINT ( 'NONE',  ( -130.5728709571500588, -24.58764167366261333, 9.439037205594624780 ) ) ;
#64617=EDGE_CURVE ( 'NONE', #49698, #623, #60364, .T. ) ;
#64619=CARTESIAN_POINT ( 'NONE',  ( -68.52210156676301267, -23.48783264082477018, -1.443836473390095243 ) ) ;
#64620=CARTESIAN_POINT ( 'NONE',  ( -15.52061920455031618, -11.66286593722069931, -1.500000000000002220 ) ) ;
#64621=CARTESIAN_POINT ( 'NONE',  ( -45.63591179856666002, -24.63355581998384736, 0.9682620441944017609 ) ) ;
#64623=CARTESIAN_POINT ( 'NONE',  ( -16.58133674543539371, -10.29093563426468450, 11.49999999999999645 ) ) ;
#64625=CARTESIAN_POINT ( 'NONE',  ( -80.48900664166535535, -25.12298712672050982, 7.101635559041870494 ) ) ;
#64626=ORIENTED_EDGE ( 'NONE', *, *, #22287, .T. ) ;
#64629=CARTESIAN_POINT ( 'NONE',  ( -89.51459311308768463, -23.96119346886881374, -0.6495511937831908167 ) ) ;
#64630=CARTESIAN_POINT ( 'NONE',  ( -90.52287095715006160, -25.00158670708909625, 2.256160236439166411 ) ) ;
#64632=CARTESIAN_POINT ( 'NONE',  ( -80.51244414166535535, -25.03156060877706324, 7.563174219299074963 ) ) ;
#64633=CARTESIAN_POINT ( 'NONE',  ( 8.085132396474181249, 17.94908993440701295, -1.500000000000002220 ) ) ;
#64636=CARTESIAN_POINT ( 'NONE',  ( -78.52287095715006160, -24.51283580621366198, 0.6167428607019652675 ) ) ;
#64637=PLANE ( 'NONE',  #35031 ) ;
#64638=B_SPLINE_CURVE_WITH_KNOTS ( 'NONE', 3,
 ( #23229, #53712, #15129, #93251, #46092, #85646 ),
 .UNSPECIFIED., .F., .F.,
 ( 4, 2, 4 ),
 ( 6.391158118964604309E-06, 0.001387004593080781809, 0.002767618028042598960 ),
 .UNSPECIFIED. ) ;
#64640=CARTESIAN_POINT ( 'NONE',  ( -91.92287095715003886, -23.47593901973090524, -1.443836447538997314 ) ) ;
#64642=CARTESIAN_POINT ( 'NONE',  ( -110.1363633712414298, -25.11151251321651046, 2.838859203344919813 ) ) ;
#64643=CARTESIAN_POINT ( 'NONE',  ( -97.63537931045868845, -23.73791477778912196, 11.05961554403170410 ) ) ;
#64644=CARTESIAN_POINT ( 'NONE',  ( -86.52287095715006160, -24.66019654487199375, 8.947790411086119278 ) ) ;
#64646=CARTESIAN_POINT ( 'NONE',  ( -69.34374060353803770, -25.24515230211321537, 6.178485843430418178 ) ) ;
#64648=CARTESIAN_POINT ( 'NONE',  ( -19.80664267627650688, 2.137978742899185214, -1.500000000000002220 ) ) ;
#64649=CARTESIAN_POINT ( 'NONE',  ( -75.59181694504910354, -24.40133493613049964, 9.663955038902805939 ) ) ;
#64650=CARTESIAN_POINT ( 'NONE',  ( -18.79335158860655142, 6.462138572525057967, -1.500000000000002220 ) ) ;
#64652=AXIS2_PLACEMENT_3D ( 'NONE', #38776, #84452, #14934 ) ;
#64653=CARTESIAN_POINT ( 'NONE',  ( -71.52287095715004739, -23.72747288104470087, -1.053458166803227236 ) ) ;
#64654=CARTESIAN_POINT ( 'NONE',  ( -50.53967329592638436, -25.13373113272038850, 7.098271152210802626 ) ) ;
#64656=CARTESIAN_POINT ( 'NONE',  ( -80.53629517725291009, -25.00182538069146787, 7.747789668545041586 ) ) ;
#64657=CARTESIAN_POINT ( 'NONE',  ( 20.60118427460899326, -2.865472796819775958, 11.49999999999999645 ) ) ;
#64659=AXIS2_PLACEMENT_3D ( 'NONE', #17958, #34687, #72255 ) ;
#64660=B_SPLINE_CURVE_WITH_KNOTS ( 'NONE', 3,
 ( #82734, #7112, #90852, #21323 ),
 .UNSPECIFIED., .F., .F.,
 ( 4, 4 ),
 ( 0.000000000000000000, 9.999999999998897304E-05 ),
 .UNSPECIFIED. ) ;
#64662=CARTESIAN_POINT ( 'NONE',  ( 7.682656365740156090, -21.48159684637525046, 11.49999999999999645 ) ) ;
#64663=ORIENTED_EDGE ( 'NONE', *, *, #80542, .F. ) ;
#64665=CARTESIAN_POINT ( 'NONE',  ( -127.5564497244640592, -23.48783264082477373, -1.443836473390084363 ) ) ;
#64666=ORIENTED_EDGE ( 'NONE', *, *, #34911, .T. ) ;
#64667=AXIS2_PLACEMENT_3D ( 'NONE', #5354, #36308, #98187 ) ;
#64668=CARTESIAN_POINT ( 'NONE',  ( -20.17641613807547785, 1.360797614858565874, -1.500000000000002220 ) ) ;
#64669=CARTESIAN_POINT ( 'NONE',  ( -55.58953762381672448, -25.00158670708909270, 2.256160236439167299 ) ) ;
#64670=CARTESIAN_POINT ( 'NONE',  ( -114.5895376238167103, -24.66019654487199730, 8.947790411086117501 ) ) ;
#64674=CARTESIAN_POINT ( 'NONE',  ( -100.6228709571500559, -24.91544648472626378, 1.928969306349431534 ) ) ;
#64675=CARTESIAN_POINT ( 'NONE',  ( 7.431233518514567926, -18.57414813805618081, -1.500000000000002220 ) ) ;
#64676=CARTESIAN_POINT ( 'NONE',  ( -12.80012119340476140, -16.60591428456014640, 11.49999999999999645 ) ) ;
#64678=CARTESIAN_POINT ( 'NONE',  ( -124.6228709571500701, -24.50321055353806443, 9.387540953477524042 ) ) ;
#64679=CARTESIAN_POINT ( 'NONE',  ( 21.95769793831392036, 2.030053023538682222, -1.500000000000002220 ) ) ;
#64680=CARTESIAN_POINT ( 'NONE',  ( -40.11299260137283795, -25.31589322304537504, 5.047402315637626202 ) ) ;
#64681=OPEN_SHELL ( 'NONE', ( #34457 ) ) ;
#64684=FACE_OUTER_BOUND ( 'NONE', #67003, .T. ) ;
#64685=CARTESIAN_POINT ( 'NONE',  ( -50.52287095715006160, -24.99132157543166599, 2.256160258750667502 ) ) ;
#64687=PLANE ( 'NONE',  #43763 ) ;
#64688=EDGE_CURVE ( 'NONE', #81281, #96245, #3383, .T. ) ;
#64690=ADVANCED_FACE ( 'NONE', ( #9091 ), #17705, .T. ) ;
#64694=DIRECTION ( 'NONE',  ( 0.000000000000000000, 0.9999999999976377785, 2.173523156925979975E-06 ) ) ;
#64695=CARTESIAN_POINT ( 'NONE',  ( 2.947869850540926429, 20.32360706268488215, -1.500000000000002220 ) ) ;
#64697=EDGE_LOOP ( 'NONE', ( #403, #37795, #75226, #43949 ) ) ;
#64700=LINE ( 'NONE', #80891, #82100 ) ;
#64701=CARTESIAN_POINT ( 'NONE',  ( 15.82088602905085750, -15.72875506571707760, -1.500000000000002220 ) ) ;
#64705=FACE_OUTER_BOUND ( 'NONE', #76523, .T. ) ;
#64706=ORIENTED_EDGE ( 'NONE', *, *, #66649, .F. ) ;
#64707=PLANE ( 'NONE',  #59854 ) ;
#64708=CARTESIAN_POINT ( 'NONE',  ( -73.52287095715013265, -23.96127896941631974, -0.6493128931038029128 ) ) ;
#64709=CARTESIAN_POINT ( 'NONE',  ( 11.47802407633690258, -17.41396394059345454, -1.500000000000002220 ) ) ;
#64712=ORIENTED_EDGE ( 'NONE', *, *, #56569, .F. ) ;
#64715=CARTESIAN_POINT ( 'NONE',  ( -69.97463645619113493, -25.03149363652662274, 7.520861778187123647 ) ) ;
#64716=CARTESIAN_POINT ( 'NONE',  ( 12.99892964944760543, 16.54660993828877125, -1.500000000000002220 ) ) ;
#64717=ORIENTED_EDGE ( 'NONE', *, *, #6081, .T. ) ;
#64718=CARTESIAN_POINT ( 'NONE',  ( -102.5228709571500758, -24.65952944569305316, 1.056160979905702346 ) ) ;
#64720=CARTESIAN_POINT ( 'NONE',  ( -108.6228709571500559, -29.50250243563736774, 8.947779886222136270 ) ) ;
#64722=CARTESIAN_POINT ( 'NONE',  ( -86.54506020849899528, -24.51419770103155926, 9.386484678747184063 ) ) ;
#64723=CARTESIAN_POINT ( 'NONE',  ( -59.51516556476029507, -23.73766607897669445, -1.055555164236460675 ) ) ;
#64724=CARTESIAN_POINT ( 'NONE',  ( 0.4029737066630413311, -21.70969715354747009, -1.500000000000002220 ) ) ;
#64726=CARTESIAN_POINT ( 'NONE',  ( -19.85906585229243504, 9.992431322412627992, 11.49999999999999645 ) ) ;
#64727=ORIENTED_EDGE ( 'NONE', *, *, #52994, .T. ) ;
#64728=CARTESIAN_POINT ( 'NONE',  ( -119.4728709571500644, -25.40558663563398056, 5.000950440326719537 ) ) ;
#64729=CARTESIAN_POINT ( 'NONE',  ( -100.6814946224345846, -25.30401792888237367, 5.197789011716578145 ) ) ;
#64730=EDGE_CURVE ( 'NONE', #61820, #93974, #63911, .T. ) ;
#64731=CARTESIAN_POINT ( 'NONE',  ( -70.65813959336661298, -25.30064099092117758, 5.349778433208494555 ) ) ;
#64732=ORIENTED_EDGE ( 'NONE', *, *, #12986, .T. ) ;
#64735=ORIENTED_EDGE ( 'NONE', *, *, #79430, .T. ) ;
#64738=ORIENTED_EDGE ( 'NONE', *, *, #72996, .T. ) ;
#64740=CARTESIAN_POINT ( 'NONE',  ( -47.58953762381671737, -24.64965694238406613, 8.947790433994660120 ) ) ;
#64742=CARTESIAN_POINT ( 'NONE',  ( -32.62287095715005592, -23.96127896941632685, -0.6493128931037921436 ) ) ;
#64743=ORIENTED_EDGE ( 'NONE', *, *, #68768, .T. ) ;
#64744=CARTESIAN_POINT ( 'NONE',  ( -130.5728709571501156, -24.71478263084194538, 9.068606591826432251 ) ) ;
#64745=CARTESIAN_POINT ( 'NONE',  ( -21.90463088927077706, -4.570550247397807908, -1.500000000000002220 ) ) ;
#64746=ORIENTED_EDGE ( 'NONE', *, *, #65277, .F. ) ;
#64747=ORIENTED_EDGE ( 'NONE', *, *, #24696, .T. ) ;
#64748=CARTESIAN_POINT ( 'NONE',  ( -34.52287095715006160, -23.95044443724991723, 10.65354141964649237 ) ) ;
#64749=CARTESIAN_POINT ( 'NONE',  ( -101.5853466808658254, -24.66019654487200086, 8.947790411086115725 ) ) ;
#64750=CARTESIAN_POINT ( 'NONE',  ( -39.56956369306367094, -25.31127738444162034, 4.659494810401162646 ) ) ;
#64751=CARTESIAN_POINT ( 'NONE',  ( -99.52287095715006160, -29.50248528299804818, 1.056150453629042030 ) ) ;
#64752=CARTESIAN_POINT ( 'NONE',  ( -30.59463558439210118, -24.75179208683297105, 8.640809912072082710 ) ) ;
#64753=EDGE_CURVE ( 'NONE', #9998, #82876, #94110, .T. ) ;
#64754=CARTESIAN_POINT ( 'NONE',  ( -19.52990877098713796, 1.257015143768854815, -1.500000000000002220 ) ) ;
#64757=CARTESIAN_POINT ( 'NONE',  ( -15.45034113870702441, -14.97902827799142500, 11.49999999999998934 ) ) ;
#64758=CARTESIAN_POINT ( 'NONE',  ( -51.29687923781919068, -25.27367468601215350, 3.993462154588707680 ) ) ;
#64759=CARTESIAN_POINT ( 'NONE',  ( -71.19450251067907232, -25.25639499143044731, 6.630762337283159447 ) ) ;
#64763=CARTESIAN_POINT ( 'NONE',  ( 15.56936346670522120, 16.85858822313069894, -1.500000000000002220 ) ) ;
#64764=AXIS2_PLACEMENT_3D ( 'NONE', #52884, #21903, #83317 ) ;
#64767=CARTESIAN_POINT ( 'NONE',  ( -129.6228709571500417, -29.50250243563736774, 8.947779886222132717 ) ) ;
#64768=CARTESIAN_POINT ( 'NONE',  ( -18.81522532469529452, 6.996975221643539911, 11.49999999999999645 ) ) ;
#64771=CARTESIAN_POINT ( 'NONE',  ( -99.52287095715011844, -23.48783264083466449, -1.443836473374706442 ) ) ;
#64772=CARTESIAN_POINT ( 'NONE',  ( -36.62287095715005592, -24.64965695001467694, 8.947790433994187609 ) ) ;
#64774=CARTESIAN_POINT ( 'NONE',  ( 15.56394622224390645, 12.30447529683395125, -1.500000000000002220 ) ) ;
#64775=CARTESIAN_POINT ( 'NONE',  ( 2.021814659504407579E-13, -19.30000000000000426, 11.49999999999999645 ) ) ;
#64776=CARTESIAN_POINT ( 'NONE',  ( 18.28535361393070957, 7.309334553982634652, -1.500000000000002220 ) ) ;
#64778=CARTESIAN_POINT ( 'NONE',  ( -41.62287095715007723, -23.73934037231756733, 11.05740245334329863 ) ) ;
#64780=CARTESIAN_POINT ( 'NONE',  ( -125.6228709571500559, -23.47596703998600631, 11.44779298504227860 ) ) ;
#64782=CARTESIAN_POINT ( 'NONE',  ( 18.09409571311175569, -9.955296453752364272, 11.49999999999999645 ) ) ;
#64786=CARTESIAN_POINT ( 'NONE',  ( -20.50338545487000275, 9.463669735852004550, 11.49999999999999645 ) ) ;
#64787=ORIENTED_EDGE ( 'NONE', *, *, #23637, .F. ) ;
#64788=CARTESIAN_POINT ( 'NONE',  ( -53.62287095715004881, -24.65952944569303895, 1.056160979905692576 ) ) ;
#64789=CARTESIAN_POINT ( 'NONE',  ( -97.59657083758668250, -23.73766607897670156, -1.055555164236452237 ) ) ;
#64790=CARTESIAN_POINT ( 'NONE',  ( -26.26041136509451590, -24.89299099432205864, 3.510312236646374373 ) ) ;
#64792=CARTESIAN_POINT ( 'NONE',  ( -26.98635835925963633, -24.61460083625618722, 8.112879358581045253 ) ) ;
#64795=ORIENTED_EDGE ( 'NONE', *, *, #64688, .F. ) ;
#64796=CARTESIAN_POINT ( 'NONE',  ( 11.81885653190370888, -19.86314957129924608, 11.49999999999999645 ) ) ;
#64797=CARTESIAN_POINT ( 'NONE',  ( 12.51456667378993259, 19.11410217522374921, -1.500000000000002220 ) ) ;
#64799=AXIS2_PLACEMENT_3D ( 'NONE', #40320, #79870, #87998 ) ;
#64801=CARTESIAN_POINT ( 'NONE',  ( -82.50294125089578756, -24.51419770103156281, 9.386484678747185839 ) ) ;
#64802=CARTESIAN_POINT ( 'NONE',  ( 12.90280524143238594, -18.44629484376132922, 11.49999999999999645 ) ) ;
#64803=ORIENTED_EDGE ( 'NONE', *, *, #40260, .F. ) ;
#64806=CARTESIAN_POINT ( 'NONE',  ( 12.42595048307055983, -18.10569578304522764, -1.500000000000002220 ) ) ;
#64807=CARTESIAN_POINT ( 'NONE',  ( -120.5228709571500616, -25.00158670708909625, 2.256160236439166411 ) ) ;
#64809=CARTESIAN_POINT ( 'NONE',  ( -111.6286677502680789, -23.96119346886881019, -0.6495511937832035843 ) ) ;
#64810=CARTESIAN_POINT ( 'NONE',  ( -29.24615158708846963, -24.79699756444347969, 5.024435584847914527 ) ) ;
#64811=VERTEX_POINT ( 'NONE', #54284 ) ;
#64812=CARTESIAN_POINT ( 'NONE',  ( -48.49448130989669892, -24.35071581493543036, 9.817618358456027039 ) ) ;
#64814=VERTEX_POINT ( 'NONE', #78085 ) ;
#64815=CARTESIAN_POINT ( 'NONE',  ( -54.65091972564611922, -23.73791477778911130, 11.05961554403171299 ) ) ;
#64817=CARTESIAN_POINT ( 'NONE',  ( 17.04084431845542369, 11.38269047019995206, 11.49999999999998934 ) ) ;
#64819=ORIENTED_EDGE ( 'NONE', *, *, #95586, .T. ) ;
#64820=ORIENTED_EDGE ( 'NONE', *, *, #11204, .T. ) ;
#64821=VERTEX_POINT ( 'NONE', #71505 ) ;
#64822=CARTESIAN_POINT ( 'NONE',  ( -50.31102424471665557, -25.31399524998115780, 5.199282048349309626 ) ) ;
#64823=CARTESIAN_POINT ( 'NONE',  ( 23.08992502549420323, -0.8469403905869224980, -1.500000000000002220 ) ) ;
#64824=CARTESIAN_POINT ( 'NONE',  ( -104.6286252005051693, -24.15620529776628800, 10.23563542870659759 ) ) ;
#64825=CARTESIAN_POINT ( 'NONE',  ( -5.305567426876419468, 19.62801697144059787, -1.500000000000002220 ) ) ;
#64826=ADVANCED_FACE ( 'NONE', ( #23299 ), #36925, .T. ) ;
#64828=CARTESIAN_POINT ( 'NONE',  ( -46.62287095715004881, -29.50247984919015209, -1.443849546365058689 ) ) ;
#64829=CARTESIAN_POINT ( 'NONE',  ( -88.62287095715004170, -23.48783264082479150, -1.443836473390063935 ) ) ;
#64830=EDGE_CURVE ( 'NONE', #54879, #95555, #37350, .T. ) ;
#64831=CARTESIAN_POINT ( 'NONE',  ( -46.58953762381672448, -24.65952944569303895, 1.056160979905690134 ) ) ;
#64833=ORIENTED_EDGE ( 'NONE', *, *, #43960, .T. ) ;
#64834=CARTESIAN_POINT ( 'NONE',  ( -28.45618646431091392, -24.76880908853930308, 2.526465311820395243 ) ) ;
#64835=CARTESIAN_POINT ( 'NONE',  ( -49.19182681462018536, -25.31573717972797866, 4.415198315518342298 ) ) ;
#64836=EDGE_CURVE ( 'NONE', #89496, #95755, #47047, .T. ) ;
#64837=ORIENTED_EDGE ( 'NONE', *, *, #37682, .F. ) ;
#64838=EDGE_CURVE ( 'NONE', #75985, #6656, #42212, .T. ) ;
#64839=CARTESIAN_POINT ( 'NONE',  ( 1.212613378922696050, -20.72488358683818888, 11.49999999999998934 ) ) ;
#64841=CARTESIAN_POINT ( 'NONE',  ( -125.5547332246454175, -24.63355581998386512, 0.9682620441944075340 ) ) ;
#64842=VERTEX_POINT ( 'NONE', #58765 ) ;
#64843=CARTESIAN_POINT ( 'NONE',  ( -41.60819791265744527, -23.73791477778911485, 11.05961554403170943 ) ) ;
#64844=LINE ( 'NONE', #95754, #59995 ) ;
#64845=ORIENTED_EDGE ( 'NONE', *, *, #20572, .F. ) ;
#64846=ORIENTED_EDGE ( 'NONE', *, *, #34733, .T. ) ;
#64848=CARTESIAN_POINT ( 'NONE',  ( -116.6228709571501270, -23.96177878511308634, 10.65340807706329684 ) ) ;
#64849=LINE ( 'NONE', #63334, #4390 ) ;
#64850=CARTESIAN_POINT ( 'NONE',  ( -16.08457400211760913, 15.13120210334024662, 11.49999999999999645 ) ) ;
#64851=ORIENTED_EDGE ( 'NONE', *, *, #16805, .T. ) ;
#64853=CARTESIAN_POINT ( 'NONE',  ( -22.56969522194696509, -0.6267768857631424995, -1.500000000000002220 ) ) ;
#64855=CARTESIAN_POINT ( 'NONE',  ( -95.62287095715005592, -23.48783264082479150, -1.443836473390061936 ) ) ;
#64856=VERTEX_POINT ( 'NONE', #12581 ) ;
#64857=EDGE_LOOP ( 'NONE', ( #43091, #51381, #40192, #32745 ) ) ;
#64860=CARTESIAN_POINT ( 'NONE',  ( -57.62780115005737258, -24.51419770103157347, 9.386484678747176957 ) ) ;
#64861=VERTEX_POINT ( 'NONE', #43049 ) ;
#64862=CARTESIAN_POINT ( 'NONE',  ( -17.86006801910157193, 11.38285951858322242, -1.500000000000002220 ) ) ;
#64867=CARTESIAN_POINT ( 'NONE',  ( -19.97062832128981213, -9.750827054148329509, -1.500000000000002220 ) ) ;
#64869=ORIENTED_EDGE ( 'NONE', *, *, #11189, .T. ) ;
#64872=VECTOR ( 'NONE', #17275, 1000.000000000000114 ) ;
#64874=LINE ( 'NONE', #26277, #1597 ) ;
#64876=CARTESIAN_POINT ( 'NONE',  ( -19.06185424839875964, 3.971334347869299286, 11.49999999999998934 ) ) ;
#64878=CARTESIAN_POINT ( 'NONE',  ( 2.169945595249806125, 21.32849103866527329, 11.49999999999998934 ) ) ;
#64880=CARTESIAN_POINT ( 'NONE',  ( -27.55569643375672584, -24.57999497573050007, 1.631374204058557043 ) ) ;
#64881=PLANE ( 'NONE',  #90841 ) ;
#64882=FACE_OUTER_BOUND ( 'NONE', #96369, .T. ) ;
#64883=CARTESIAN_POINT ( 'NONE',  ( -16.51154719052397724, 15.62863258182435189, -1.500000000000002220 ) ) ;
#64885=CARTESIAN_POINT ( 'NONE',  ( -98.58489604146052443, -24.65952944569305316, 1.056160979905700570 ) ) ;
#64886=CARTESIAN_POINT ( 'NONE',  ( -103.5228709571500758, -23.47596703998600631, 11.44779298504228215 ) ) ;
#64887=CARTESIAN_POINT ( 'NONE',  ( 18.06118663784855372, 8.336529998961283994, 11.49999999999999645 ) ) ;
#64888=DIRECTION ( 'NONE',  ( -3.773278334453080206E-23, 0.9999999999976377785, 2.173523156925979975E-06 ) ) ;
#64890=CARTESIAN_POINT ( 'NONE',  ( -48.58720723522154827, -24.34968618360933590, 0.1864209137778884418 ) ) ;
#64891=ORIENTED_EDGE ( 'NONE', *, *, #98087, .T. ) ;
#64892=DIRECTION ( 'NONE',  ( -1.000000000000000000, -3.773278334444167608E-23, -8.201307833595939069E-29 ) ) ;
#64893=EDGE_CURVE ( 'NONE', #31485, #46589, #19684, .T. ) ;
#64894=CARTESIAN_POINT ( 'NONE',  ( -31.82673689144044360, -24.87479601683088148, 8.247789944647561100 ) ) ;
#64895=CARTESIAN_POINT ( 'NONE',  ( -14.16021466491576675, 16.42052772630311352, 11.49999999999998934 ) ) ;
#64896=CARTESIAN_POINT ( 'NONE',  ( -51.60933002250928325, -25.14098292474398377, 7.057872611485954906 ) ) ;
#64897=CARTESIAN_POINT ( 'NONE',  ( -4.154358412494840280, 19.03220294597612039, -1.500000000000002220 ) ) ;
#64899=ORIENTED_EDGE ( 'NONE', *, *, #89891, .T. ) ;
#64900=B_SPLINE_CURVE_WITH_KNOTS ( 'NONE', 3,
 ( #5511, #22223, #66936, #53204 ),
 .UNSPECIFIED., .F., .F.,
 ( 4, 4 ),
 ( 3.469446951953614189E-18, 0.0001002978978728838905 ),
 .UNSPECIFIED. ) ;
#64903=CARTESIAN_POINT ( 'NONE',  ( 18.81987132735423174, -8.002443037797982939, 11.49999999999999645 ) ) ;
#64906=LINE ( 'NONE', #27805, #62630 ) ;
#64907=ORIENTED_EDGE ( 'NONE', *, *, #9452, .F. ) ;
#64910=CARTESIAN_POINT ( 'NONE',  ( -39.18717306657202215, -25.31628593408776595, 4.881706631208792224 ) ) ;
#64912=CARTESIAN_POINT ( 'NONE',  ( -109.6247177088518896, -24.51314013834315730, 0.6176544820404190617 ) ) ;
#64913=ORIENTED_EDGE ( 'NONE', *, *, #63727, .T. ) ;
#64914=CARTESIAN_POINT ( 'NONE',  ( -66.49287662190819503, -24.66019654487199375, 8.947790411086119278 ) ) ;
#64915=CARTESIAN_POINT ( 'NONE',  ( -22.60589916338503613, 3.847557683979087706, 11.49999999999999645 ) ) ;
#64916=CARTESIAN_POINT ( 'NONE',  ( -2.780358639097238349, 22.57001311929844434, -1.500000000000002220 ) ) ;
#64918=CARTESIAN_POINT ( 'NONE',  ( -122.6228709571500417, -23.47593901973091235, -1.443836447538997536 ) ) ;
#64919=CARTESIAN_POINT ( 'NONE',  ( -90.58763920575688644, -24.63355581998384380, 0.9682620441943978751 ) ) ;
#64920=CARTESIAN_POINT ( 'NONE',  ( -125.2228709571500644, -23.47593901973090524, -1.443836447538996426 ) ) ;
#64921=CARTESIAN_POINT ( 'NONE',  ( -44.55620429048338593, -23.48783264082477373, -1.443836473390073261 ) ) ;
#64922=VECTOR ( 'NONE', #6379, 1000.000000000000114 ) ;
#64923=CARTESIAN_POINT ( 'NONE',  ( -21.72861685410901700, 2.547970858986955189, 11.49999999999998934 ) ) ;
#64924=B_SPLINE_CURVE_WITH_KNOTS ( 'NONE', 3,
 ( #90023, #97134, #20993, #98115, #80411, #89030, #73308, #58579, #81910, #74782, #81415, #12388, #89522, #12880 ),
 .UNSPECIFIED., .F., .F.,
 ( 4, 2, 2, 2, 2, 2, 4 ),
 ( 7.059813062317230268E-18, 0.0002389841638349673222, 0.0004779683276699275970, 0.0009559366553398477130, 0.001433904983009767937, 0.001672889146844726803, 0.001911873310679685885 ),
 .UNSPECIFIED. ) ;
#64925=CARTESIAN_POINT ( 'NONE',  ( -69.58396311289207858, -24.51419770103157347, 9.386484678747178734 ) ) ;
#64926=CARTESIAN_POINT ( 'NONE',  ( -49.04145601308662350, -25.30525654051268702, 5.514141841267435673 ) ) ;
#64930=CARTESIAN_POINT ( 'NONE',  ( -8.052747710315523832, 18.77774781879659116, -1.500000000000002220 ) ) ;
#64931=ORIENTED_EDGE ( 'NONE', *, *, #75926, .T. ) ;
#64933=CARTESIAN_POINT ( 'NONE',  ( 14.87233727408824713, -17.56007624320114857, -1.500000000000002220 ) ) ;
#64940=CARTESIAN_POINT ( 'NONE',  ( -53.62803857038250044, -24.51419770103157347, 9.386484678747180510 ) ) ;
#64941=CARTESIAN_POINT ( 'NONE',  ( -18.12654925440673637, -11.31956730046968751, 11.49999999999999645 ) ) ;
#64943=ADVANCED_FACE ( 'NONE', ( #10586 ), #81604, .T. ) ;
#64946=CARTESIAN_POINT ( 'NONE',  ( -18.24902840909259538, -12.68162010772806170, -1.500000000000002220 ) ) ;
#64947=EDGE_CURVE ( 'NONE', #61568, #88227, #26320, .T. ) ;
#64948=CARTESIAN_POINT ( 'NONE',  ( 15.58315679939408582, 13.61395703526229894, 11.49999999999998934 ) ) ;
#64949=B_SPLINE_CURVE_WITH_KNOTS ( 'NONE', 3,
 ( #71162, #73166, #86872, #1652, #33594, #79256, #32588, #3163, #88384, #71663 ),
 .UNSPECIFIED., .F., .F.,
 ( 4, 2, 2, 2, 4 ),
 ( 5.204170427930421283E-18, 0.0002155461666041007132, 0.0004310923332081962223, 0.0006466384998122917584, 0.0008621846664163872404 ),
 .UNSPECIFIED. ) ;
#64951=ORIENTED_EDGE ( 'NONE', *, *, #88714, .T. ) ;
#64953=CARTESIAN_POINT ( 'NONE',  ( -69.85571445902073151, -25.30060019737137367, 6.009288023823078362 ) ) ;
#64954=ORIENTED_EDGE ( 'NONE', *, *, #64488, .T. ) ;
#64955=CARTESIAN_POINT ( 'NONE',  ( -129.6228709571500417, -29.50250243563736774, 8.947779886222132717 ) ) ;
#64958=CARTESIAN_POINT ( 'NONE',  ( 12.60132613692001691, 16.66296579206088069, -1.500000000000002220 ) ) ;
#64959=EDGE_CURVE ( 'NONE', #80762, #41069, #32485, .T. ) ;
#64960=CARTESIAN_POINT ( 'NONE',  ( 21.14253370195585546, 5.708146584608840612, 11.49999999999999645 ) ) ;
#64962=FACE_OUTER_BOUND ( 'NONE', #42007, .T. ) ;
#64964=CARTESIAN_POINT ( 'NONE',  ( -1.726696889551340153, 22.42386595106472669, -1.500000000000002220 ) ) ;
#64965=CARTESIAN_POINT ( 'NONE',  ( 19.98859412959824411, 6.261702723725245612, -1.500000000000002220 ) ) ;
#64966=CARTESIAN_POINT ( 'NONE',  ( -26.22762954581084571, -24.88148982559359723, 6.176716197550690346 ) ) ;
#64968=CARTESIAN_POINT ( 'NONE',  ( -121.6228709571500417, -23.47593901973091235, -1.443836447538997536 ) ) ;
#64969=ORIENTED_EDGE ( 'NONE', *, *, #47260, .F. ) ;
#64970=ORIENTED_EDGE ( 'NONE', *, *, #16073, .F. ) ;
#64972=CARTESIAN_POINT ( 'NONE',  ( -52.62368446719793269, -24.65952944569304606, 1.056160979905696573 ) ) ;
#64974=CARTESIAN_POINT ( 'NONE',  ( 11.27511198983438412, 18.17944245918264912, -1.500000000000002220 ) ) ;
#64975=EDGE_LOOP ( 'NONE', ( #40996, #4598, #86510, #29618 ) ) ;
#64976=CARTESIAN_POINT ( 'NONE',  ( -28.62287095715004881, -23.31957264754183967, 11.44779298504227860 ) ) ;
#64977=CARTESIAN_POINT ( 'NONE',  ( 17.50165659415881336, 11.77592616506222711, 11.49999999999998934 ) ) ;
#64978=CARTESIAN_POINT ( 'NONE',  ( -30.44146006906462532, -24.26584525523073665, 9.960304333224314632 ) ) ;
#64981=CARTESIAN_POINT ( 'NONE',  ( -101.5089468450591994, -24.65952944569305316, 1.056160979905706121 ) ) ;
#64982=CARTESIAN_POINT ( 'NONE',  ( -109.5706907882233025, -25.31518732623182899, 4.855924937824241283 ) ) ;
#64983=CARTESIAN_POINT ( 'NONE',  ( 19.90762846840230083, -9.494064324355022677, -1.500000000000002220 ) ) ;
#64984=ORIENTED_EDGE ( 'NONE', *, *, #37521, .F. ) ;
#64985=CARTESIAN_POINT ( 'NONE',  ( -65.49046995964316409, -24.73531770709095312, 8.716586749053508498 ) ) ;
#64987=CARTESIAN_POINT ( 'NONE',  ( -60.62578254086317742, -24.92564183028978420, 1.928384488918252648 ) ) ;
#64989=CARTESIAN_POINT ( 'NONE',  ( -25.51202922834713149, -24.77321340604576960, 7.214475432169975555 ) ) ;
#64992=CARTESIAN_POINT ( 'NONE',  ( -0.3244385709253747585, -21.36021439428519386, -1.500000000000002220 ) ) ;
#64993=CARTESIAN_POINT ( 'NONE',  ( -81.52287095715009002, -24.50216790748205398, 0.6166512839542526159 ) ) ;
#64994=CARTESIAN_POINT ( 'NONE',  ( -52.58953762381672448, -23.48783264082478794, -1.443836473390070596 ) ) ;
#64996=ADVANCED_FACE ( 'NONE', ( #42059 ), #45048, .F. ) ;
#64999=CARTESIAN_POINT ( 'NONE',  ( 0.2737972009257602091, 22.58959237946467624, -1.500000000000002220 ) ) ;
#65000=CARTESIAN_POINT ( 'NONE',  ( -112.6228709571500559, -23.47593901973091235, -1.443836447538999312 ) ) ;
#65001=ORIENTED_EDGE ( 'NONE', *, *, #42111, .F. ) ;
#65002=CARTESIAN_POINT ( 'NONE',  ( -50.51965600136372103, -25.31394903530583917, 5.202396475616230198 ) ) ;
#65003=FACE_OUTER_BOUND ( 'NONE', #32112, .T. ) ;
#65004=CARTESIAN_POINT ( 'NONE',  ( 18.24634267693259559, -7.554628487255452107, 11.49999999999999645 ) ) ;
#65005=CARTESIAN_POINT ( 'NONE',  ( -93.52287095715006160, -23.48786465467241769, 11.44779295918254292 ) ) ;
#65006=B_SPLINE_CURVE_WITH_KNOTS ( 'NONE', 3,
 ( #81294, #50355, #34631, #65600 ),
 .UNSPECIFIED., .F., .F.,
 ( 4, 4 ),
 ( 0.000000000000000000, 0.0001000000000000167422 ),
 .UNSPECIFIED. ) ;
#65007=CARTESIAN_POINT ( 'NONE',  ( -67.60891996484096467, -23.48783264082477018, -1.443836473390094799 ) ) ;
#65008=ORIENTED_EDGE ( 'NONE', *, *, #44738, .F. ) ;
#65009=PLANE ( 'NONE',  #87937 ) ;
#65010=CARTESIAN_POINT ( 'NONE',  ( -99.55620429048339304, -24.66019654487199730, 8.947790411086124607 ) ) ;
#65012=CARTESIAN_POINT ( 'NONE',  ( -13.01863397230089170, 17.21462230531794901, 11.49999999999998934 ) ) ;
#65013=CARTESIAN_POINT ( 'NONE',  ( -91.52287095715006160, -23.47593901973090524, -1.443836447538996648 ) ) ;
#65014=CARTESIAN_POINT ( 'NONE',  ( -76.62287095715007013, -24.66019654487199730, 8.947790411086128159 ) ) ;
#65016=DIRECTION ( 'NONE',  ( -3.773278334453080206E-23, 0.9999999999976377785, 2.173523156925979975E-06 ) ) ;
#65017=CARTESIAN_POINT ( 'NONE',  ( -17.81549539028256746, -8.563599010019245839, -1.500000000000002220 ) ) ;
#65018=AXIS2_PLACEMENT_3D ( 'NONE', #31249, #24136, #55103 ) ;
#65019=ORIENTED_EDGE ( 'NONE', *, *, #15465, .F. ) ;
#65021=CARTESIAN_POINT ( 'NONE',  ( 8.375906630400100639, -18.44307005126401933, 11.49999999999999645 ) ) ;
#65023=EDGE_CURVE ( 'NONE', #41151, #35233, #75966, .T. ) ;
#65025=EDGE_LOOP ( 'NONE', ( #46511, #20389, #10655, #100184 ) ) ;
#65026=CARTESIAN_POINT ( 'NONE',  ( -67.52287095715006160, -24.66019654487199730, 8.947790411086115725 ) ) ;
#65027=CARTESIAN_POINT ( 'NONE',  ( -99.58039134064964060, -25.28222918948337039, 4.246872970242233869 ) ) ;
#65029=PLANE ( 'NONE',  #14291 ) ;
#65031=CARTESIAN_POINT ( 'NONE',  ( -32.07722060962682775, -25.11010177581465186, 2.831122766525584478 ) ) ;
#65032=CARTESIAN_POINT ( 'NONE',  ( 14.85562765054232059, -13.46834898924134372, -1.500000000000002220 ) ) ;
#65033=PLANE ( 'NONE',  #83967 ) ;
#65035=EDGE_CURVE ( 'NONE', #39486, #10502, #50641, .T. ) ;
#65036=B_SPLINE_CURVE_WITH_KNOTS ( 'NONE', 3,
 ( #79479, #71883, #18574, #3379, #65783, #33300, #96698, #95210 ),
 .UNSPECIFIED., .F., .F.,
 ( 4, 2, 2, 4 ),
 ( 0.000000000000000000, 0.002001079623178230599, 0.003001619434767341561, 0.004002159246356452524 ),
 .UNSPECIFIED. ) ;
#65037=CARTESIAN_POINT ( 'NONE',  ( -51.52287095715004739, -23.73907113216990084, -1.053371485793254791 ) ) ;
#65038=FACE_OUTER_BOUND ( 'NONE', #80503, .T. ) ;
#65039=CARTESIAN_POINT ( 'NONE',  ( -80.15554980868958523, -25.30558339281096636, 4.989559503397144269 ) ) ;
#65040=B_SPLINE_CURVE_WITH_KNOTS ( 'NONE', 3,
 ( #21260, #29384, #43622, #38001 ),
 .UNSPECIFIED., .F., .F.,
 ( 4, 4 ),
 ( 0.000000000000000000, 1.000000000000000000 ),
 .UNSPECIFIED. ) ;
#65042=CARTESIAN_POINT ( 'NONE',  ( -100.7591363217603231, -25.11633374933415652, 2.865693444292612746 ) ) ;
#65044=CARTESIAN_POINT ( 'NONE',  ( -84.62287095715005592, -24.64898659630367561, 1.056161002820826145 ) ) ;
#65045=ORIENTED_EDGE ( 'NONE', *, *, #33047, .T. ) ;
#65046=CARTESIAN_POINT ( 'NONE',  ( -19.38859340154505873, -6.080128201517944753, -1.500000000000002220 ) ) ;
#65047=VERTEX_POINT ( 'NONE', #90709 ) ;
#65050=CARTESIAN_POINT ( 'NONE',  ( -118.5562042904834072, -23.47596703998600631, 11.44779298504227683 ) ) ;
#65051=ORIENTED_EDGE ( 'NONE', *, *, #6915, .F. ) ;
#65052=CARTESIAN_POINT ( 'NONE',  ( -127.6228709571500559, -29.50247984919015209, -1.443849546365044922 ) ) ;
#65053=B_SPLINE_CURVE_WITH_KNOTS ( 'NONE', 3,
 ( #18349, #17852, #88363, #80247 ),
 .UNSPECIFIED., .F., .F.,
 ( 4, 4 ),
 ( 0.000000000000000000, 1.000000000000000000 ),
 .UNSPECIFIED. ) ;
#65055=LINE ( 'NONE', #2636, #44796 ) ;
#65056=CARTESIAN_POINT ( 'NONE',  ( 13.55612473118199723, -16.30799122071102403, 11.49999999999999645 ) ) ;
#65057=CARTESIAN_POINT ( 'NONE',  ( 4.116201370682176730, 21.75534844777131838, -1.500000000000002220 ) ) ;
#65058=VECTOR ( 'NONE', #82551, 1000.000000000000227 ) ;
#65059=EDGE_CURVE ( 'NONE', #33073, #49749, #90210, .T. ) ;
#65060=CARTESIAN_POINT ( 'NONE',  ( 18.80685554986811070, -8.408966509905500430, -1.500000000000002220 ) ) ;
#65061=EDGE_LOOP ( 'NONE', ( #82316, #86117, #49587, #86317 ) ) ;
#65062=FACE_OUTER_BOUND ( 'NONE', #36134, .T. ) ;
#65063=ORIENTED_EDGE ( 'NONE', *, *, #77633, .F. ) ;
#65065=CARTESIAN_POINT ( 'NONE',  ( -50.52287095715006870, -24.51254535375842636, 9.355368624242256459 ) ) ;
#65072=CARTESIAN_POINT ( 'NONE',  ( 20.68991284688621946, 0.5745778482356619365, -1.500000000000002220 ) ) ;
#65073=EDGE_CURVE ( 'NONE', #14044, #41241, #86930, .T. ) ;
#65074=CARTESIAN_POINT ( 'NONE',  ( 2.849777056880220982, 21.50153301832798647, 11.49999999999999645 ) ) ;
#65075=EDGE_LOOP ( 'NONE', ( #88784, #51610, #86168, #12312 ) ) ;
#65076=CARTESIAN_POINT ( 'NONE',  ( -127.5228709571500616, -24.65952944569304606, 1.056160979905707675 ) ) ;
#65077=CARTESIAN_POINT ( 'NONE',  ( -28.62287095715004881, -23.33150569529546914, 11.44779297407613150 ) ) ;
#65078=CARTESIAN_POINT ( 'NONE',  ( -12.73782554413503654, -18.45060914899308457, 11.49999999999998934 ) ) ;
#65079=EDGE_CURVE ( 'NONE', #86743, #63165, #13058, .T. ) ;
#65080=CARTESIAN_POINT ( 'NONE',  ( -93.52287095715006160, -23.47593901973090524, -1.443836447538996648 ) ) ;
#65087=VERTEX_POINT ( 'NONE', #52150 ) ;
#65088=ORIENTED_EDGE ( 'NONE', *, *, #62771, .F. ) ;
#65089=CARTESIAN_POINT ( 'NONE',  ( -103.6228709571500559, -24.64898659630368627, 1.056161002820829697 ) ) ;
#65090=VERTEX_POINT ( 'NONE', #13070 ) ;
#65091=CARTESIAN_POINT ( 'NONE',  ( -18.66175431467001999, 10.11895122522205526, -1.500000000000002220 ) ) ;
#65092=EDGE_LOOP ( 'NONE', ( #88672, #7918, #63832, #91836 ) ) ;
#65093=FACE_OUTER_BOUND ( 'NONE', #31575, .T. ) ;
#65094=CARTESIAN_POINT ( 'NONE',  ( 8.176594470695947692, -20.27425322898990601, -1.500000000000002220 ) ) ;
#65095=CARTESIAN_POINT ( 'NONE',  ( -52.65164253565483676, -23.73791477778911840, 11.05961554403171299 ) ) ;
#65096=CARTESIAN_POINT ( 'NONE',  ( -40.84535658588885099, -25.18430885309796352, 3.358264732341272651 ) ) ;
#65097=DIRECTION ( 'NONE',  ( -3.773278334453079618E-23, 0.9999999999976377785, 2.173523156925979975E-06 ) ) ;
#65098=CARTESIAN_POINT ( 'NONE',  ( 18.42579859434530931, 11.83097890990371148, -1.500000000000002220 ) ) ;
#65100=ORIENTED_EDGE ( 'NONE', *, *, #91665, .F. ) ;
#65101=CARTESIAN_POINT ( 'NONE',  ( -69.62287095715005592, -24.34917612406838572, 0.1852690917426620121 ) ) ;
#65104=CARTESIAN_POINT ( 'NONE',  ( -30.57692235644935153, -25.30655462701041714, 5.551177274637566939 ) ) ;
#65106=CARTESIAN_POINT ( 'NONE',  ( -113.5562042904833930, -23.47593901973091235, -1.443836447538999312 ) ) ;
#65107=CARTESIAN_POINT ( 'NONE',  ( -82.50964971285777949, -24.15543982623907482, -0.2315651400026498552 ) ) ;
#65108=CARTESIAN_POINT ( 'NONE',  ( -12.22836702412972087, 17.35733969022439993, 11.49999999999998934 ) ) ;
#65109=LINE ( 'NONE', #86911, #85484 ) ;
#65110=CARTESIAN_POINT ( 'NONE',  ( -130.5728709571500588, -24.88273649812091293, 8.549170486301877148 ) ) ;
#65112=CARTESIAN_POINT ( 'NONE',  ( -129.5228709571500758, -24.65952944569305316, 1.056160979905707675 ) ) ;
#65113=CARTESIAN_POINT ( 'NONE',  ( -18.68671320864135765, 5.291888989699490509, -1.500000000000002220 ) ) ;
#65114=ADVANCED_FACE ( 'NONE', ( #5471 ), #84587, .T. ) ;
#65115=AXIS2_PLACEMENT_3D ( 'NONE', #51095, #75405, #60211 ) ;
#65116=CARTESIAN_POINT ( 'NONE',  ( -45.47189084317965069, -25.00158670708910336, 2.256160236439225031 ) ) ;
#65117=VERTEX_POINT ( 'NONE', #53159 ) ;
#65118=CARTESIAN_POINT ( 'NONE',  ( 18.62133539762988121, 6.091496293051981148, 11.49999999999999645 ) ) ;
#65122=CARTESIAN_POINT ( 'NONE',  ( -97.52287095715010423, -23.48783264082477018, -1.443836473390087027 ) ) ;
#65123=CARTESIAN_POINT ( 'NONE',  ( -89.51148841281252544, -24.15543982623907837, -0.2315651400026483009 ) ) ;
#65125=CARTESIAN_POINT ( 'NONE',  ( -89.40841769935767047, -25.06732983082694943, 7.447789526168953955 ) ) ;
#65126=CARTESIAN_POINT ( 'NONE',  ( 18.75866648459458830, -6.009157199652424453, -1.500000000000002220 ) ) ;
#65129=CARTESIAN_POINT ( 'NONE',  ( -94.62287095715002749, -23.72747288104469732, -1.053458166803225682 ) ) ;
#65130=DIRECTION ( 'NONE',  ( 1.000000000000000000, 3.773278334444167608E-23, 8.201307833595939069E-29 ) ) ;
#65131=B_SPLINE_CURVE_WITH_KNOTS ( 'NONE', 3,
 ( #35699, #20452, #66675, #82853, #51425, #44316 ),
 .UNSPECIFIED., .F., .F.,
 ( 4, 2, 4 ),
 ( 0.000000000000000000, 0.001380901958385387677, 0.002761803916770775354 ),
 .UNSPECIFIED. ) ;
#65134=ORIENTED_EDGE ( 'NONE', *, *, #66305, .F. ) ;
#65135=FACE_OUTER_BOUND ( 'NONE', #56441, .T. ) ;
#65137=CARTESIAN_POINT ( 'NONE',  ( -47.53539927575063473, -24.51314013834316086, 0.6176544820404172853 ) ) ;
#65138=CARTESIAN_POINT ( 'NONE',  ( -105.6228709571500559, -24.92604778743017491, 8.074972756849359001 ) ) ;
#65139=CARTESIAN_POINT ( 'NONE',  ( -79.91920829509126634, -25.20144873054373136, 6.835696071488102099 ) ) ;
#65141=CARTESIAN_POINT ( 'NONE',  ( -69.51029376924685721, -25.24515128556519272, 5.710789870928137724 ) ) ;
#65142=DIRECTION ( 'NONE',  ( 1.000000000000000000, 3.773278334444167608E-23, 8.201307833595939069E-29 ) ) ;
#65143=CARTESIAN_POINT ( 'NONE',  ( 10.26108024787556516, -17.11367029881254709, 11.49999999999998934 ) ) ;
#65144=FACE_OUTER_BOUND ( 'NONE', #17585, .T. ) ;
#65145=CARTESIAN_POINT ( 'NONE',  ( -9.044204435542846809, 17.70297415775587169, -1.500000000000002220 ) ) ;
#65148=DIRECTION ( 'NONE',  ( 0.000000000000000000, 2.173523156925980399E-06, -0.9999999999976378895 ) ) ;
#65149=EDGE_CURVE ( 'NONE', #41451, #65090, #37921, .T. ) ;
#65150=B_SPLINE_CURVE_WITH_KNOTS ( 'NONE', 3,
 ( #88587, #41924, #65770, #87076 ),
 .UNSPECIFIED., .F., .F.,
 ( 4, 4 ),
 ( 0.000000000000000000, 9.999999999998897304E-05 ),
 .UNSPECIFIED. ) ;
#65151=VECTOR ( 'NONE', #54771, 1000.000000000000114 ) ;
#65153=EDGE_CURVE ( 'NONE', #8482, #40343, #86590, .T. ) ;
#65154=CARTESIAN_POINT ( 'NONE',  ( -51.27260140835372937, -25.18295898317592219, 6.794811910356732376 ) ) ;
#65155=CARTESIAN_POINT ( 'NONE',  ( -93.62287095715005592, -24.66019654487199730, 8.947790411086124607 ) ) ;
#65156=CARTESIAN_POINT ( 'NONE',  ( -80.62685887991092670, -24.83644354573579349, 8.397322867130101898 ) ) ;
#65157=CARTESIAN_POINT ( 'NONE',  ( -8.262104503270727207, -19.10415460921518971, 11.49999999999999645 ) ) ;
#65159=CARTESIAN_POINT ( 'NONE',  ( -60.22287095715005023, -23.47593901973090169, -1.443836447538997536 ) ) ;
#65160=CARTESIAN_POINT ( 'NONE',  ( -21.14637036216210575, 8.611126525438130841, 11.49999999999999645 ) ) ;
#65161=EDGE_LOOP ( 'NONE', ( #59445, #67092, #64472, #15493 ) ) ;
#65164=ORIENTED_EDGE ( 'NONE', *, *, #24661, .F. ) ;
#65165=CARTESIAN_POINT ( 'NONE',  ( 2.165584020960389822, 20.11889322763239107, 11.49999999999998934 ) ) ;
#65169=CARTESIAN_POINT ( 'NONE',  ( -84.52287095715007581, -24.33832256527049509, 0.1851278514138626485 ) ) ;
#65170=ORIENTED_EDGE ( 'NONE', *, *, #3725, .F. ) ;
#65171=CARTESIAN_POINT ( 'NONE',  ( -109.5562042904833504, -24.64965694238575367, 8.947790433994187609 ) ) ;
#65173=CARTESIAN_POINT ( 'NONE',  ( -3.050325703546597822, 19.74810961616558913, -1.500000000000002220 ) ) ;
#65174=CARTESIAN_POINT ( 'NONE',  ( 18.73254098450790295, -9.497730595714260815, 11.49999999999999645 ) ) ;
#65176=FACE_OUTER_BOUND ( 'NONE', #23357, .T. ) ;
#65177=CARTESIAN_POINT ( 'NONE',  ( 19.90762846840230083, -9.494064324355022677, 11.49999999999998934 ) ) ;
#65180=EDGE_LOOP ( 'NONE', ( #92468, #8498, #51396, #24234 ) ) ;
#65183=FACE_OUTER_BOUND ( 'NONE', #1783, .T. ) ;
#65185=CARTESIAN_POINT ( 'NONE',  ( -72.64440388517061820, -23.73766607897670156, -1.055555164236458454 ) ) ;
#65186=CARTESIAN_POINT ( 'NONE',  ( -86.58953762381669605, -24.65952944569304606, 1.056160979905697239 ) ) ;
#65187=ORIENTED_EDGE ( 'NONE', *, *, #91076, .F. ) ;
#65188=VERTEX_POINT ( 'NONE', #87092 ) ;
#65190=CARTESIAN_POINT ( 'NONE',  ( -101.1026865405329147, -25.10935838865034597, 2.999872854746632900 ) ) ;
#65192=CARTESIAN_POINT ( 'NONE',  ( 15.48611046165106941, -13.43736321338083783, -1.500000000000002220 ) ) ;
#65193=ADVANCED_FACE ( 'NONE', ( #93196 ), #85087, .F. ) ;
#65195=CARTESIAN_POINT ( 'NONE',  ( -80.88924702628075636, -29.50249297023137629, 4.592912097770885715 ) ) ;
#65197=CARTESIAN_POINT ( 'NONE',  ( -103.6228709571500559, -24.64965695001469115, 8.947790433994178727 ) ) ;
#65198=CARTESIAN_POINT ( 'NONE',  ( -1.228339276683141579, -22.28195500894762660, -1.500000000000002220 ) ) ;
#65199=EDGE_CURVE ( 'NONE', #27742, #87028, #100202, .T. ) ;
#65201=CARTESIAN_POINT ( 'NONE',  ( -122.2228709571500502, -23.47596703998600631, 11.44779298504227860 ) ) ;
#65202=VERTEX_POINT ( 'NONE', #76965 ) ;
#65204=CARTESIAN_POINT ( 'NONE',  ( -42.62287095715004881, -24.64898659630367561, 1.056161002820819261 ) ) ;
#65205=CARTESIAN_POINT ( 'NONE',  ( -51.69691692161301688, -25.27141761418660337, 4.090265752574888225 ) ) ;
#65207=CARTESIAN_POINT ( 'NONE',  ( -19.30504728598367237, -7.930543132070424051, 11.49999999999998934 ) ) ;
#65209=ORIENTED_EDGE ( 'NONE', *, *, #94958, .F. ) ;
#65210=CARTESIAN_POINT ( 'NONE',  ( -74.52287095715007581, -23.48783264082476308, -1.443836473390090802 ) ) ;
#65213=CARTESIAN_POINT ( 'NONE',  ( -69.47374562227740569, -25.25935290055894100, 7.284000681396445742 ) ) ;
#65214=CARTESIAN_POINT ( 'NONE',  ( 3.661087877195506213, -20.73962600213626217, -1.500000000000002220 ) ) ;
#65215=ORIENTED_EDGE ( 'NONE', *, *, #88602, .F. ) ;
#65216=DIRECTION ( 'NONE',  ( -3.773278334453079030E-23, 0.9999999999976377785, 2.173523156925979128E-06 ) ) ;
#65217=CARTESIAN_POINT ( 'NONE',  ( -37.52287095715006870, -23.47596703998600631, 11.44779298504229281 ) ) ;
#65218=CARTESIAN_POINT ( 'NONE',  ( -103.6228709571500559, -29.50248528299804818, 1.056150453629042030 ) ) ;
#65219=B_SPLINE_CURVE_WITH_KNOTS ( 'NONE', 3,
 ( #9603, #54792, #70506, #79107, #31439, #85727, #997, #93837, #77599, #78095, #40563, #94333, #62400, #38552, #1503, #56302, #92829, #86226, #31945, #93329, #8609, #17211, #55297, #9101, #39051, #23312 ),
 .UNSPECIFIED., .F., .F.,
 ( 4, 2, 2, 2, 2, 2, 2, 2, 2, 2, 2, 2, 4 ),
 ( 6.348815807395609649E-06, 0.001695567397426964206, 0.002540176688236749167, 0.003384785979046533045, 0.004229395269856312152, 0.005074004560666090825, 0.006763223142285652509, 0.007607832433095433784, 0.008452441723905215060, 0.01014166030552477935, 0.01098626959633456149, 0.01183087888714434363, 0.01352009746876390618 ),
 .UNSPECIFIED. ) ;
#65220=CARTESIAN_POINT ( 'NONE',  ( -101.6955034991685238, -25.25419416351397217, 6.928825754601663611 ) ) ;
#65221=LINE ( 'NONE', #5280, #98336 ) ;
#65222=CARTESIAN_POINT ( 'NONE',  ( 19.61570337458852364, 9.273991169892711994, -1.500000000000002220 ) ) ;
#65223=CARTESIAN_POINT ( 'NONE',  ( -80.94627791849588050, -25.12224370068017620, 7.000535761828535541 ) ) ;
#65224=CARTESIAN_POINT ( 'NONE',  ( -22.27612280437926273, 0.2766752662994830247, 11.49999999999999645 ) ) ;
#65225=VERTEX_POINT ( 'NONE', #69370 ) ;
#65226=CARTESIAN_POINT ( 'NONE',  ( -50.72223433783125301, -25.24728732082473570, 5.237078820334065909 ) ) ;
#65228=CARTESIAN_POINT ( 'NONE',  ( -69.55620429048339304, -23.48786465467241058, 11.44779295918255002 ) ) ;
#65236=B_SPLINE_CURVE_WITH_KNOTS ( 'NONE', 3,
 ( #51472, #99117, #5285, #90028, #37239, #28626 ),
 .UNSPECIFIED., .F., .F.,
 ( 4, 2, 4 ),
 ( 6.391158118959990520E-06, 0.001387004593080779424, 0.002767618028042598960 ),
 .UNSPECIFIED. ) ;
#65237=B_SPLINE_CURVE_WITH_KNOTS ( 'NONE', 3,
 ( #34654, #87428, #73218, #18421 ),
 .UNSPECIFIED., .F., .F.,
 ( 4, 4 ),
 ( 0.4991261060968514851, 0.5001268531376167337 ),
 .UNSPECIFIED. ) ;
#65239=CARTESIAN_POINT ( 'NONE',  ( -32.62287095715007013, -24.34917612406838217, 0.1852690917426584039 ) ) ;
#65241=CARTESIAN_POINT ( 'NONE',  ( -130.5728709571500303, -25.10882183463795414, 2.294997381946255022 ) ) ;
#65242=CARTESIAN_POINT ( 'NONE',  ( -10.09097066620046235, 20.03973272787133553, -1.500000000000002220 ) ) ;
#65243=VERTEX_POINT ( 'NONE', #9468 ) ;
#65244=CARTESIAN_POINT ( 'NONE',  ( -89.40841769935764205, -25.19340450609639603, 6.757884810842872625 ) ) ;
#65245=CARTESIAN_POINT ( 'NONE',  ( -96.52287095715006160, -23.48786465467241769, 11.44779295918254114 ) ) ;
#65247=B_SPLINE_CURVE_WITH_KNOTS ( 'NONE', 3,
 ( #7818, #94549, #24538, #23021, #46890, #30660, #76812, #25038, #61630, #85947, #70224, #84939, #15424, #40274, #704, #31651 ),
 .UNSPECIFIED., .F., .F.,
 ( 4, 2, 2, 2, 2, 2, 2, 4 ),
 ( 0.000000000000000000, 0.0002745580509702497183, 0.0005491161019404994367, 0.0008236741529107492093, 0.001098232203880998873, 0.001647348305821530077, 0.001921906356791795679, 0.002196464407762061498 ),
 .UNSPECIFIED. ) ;
#65249=CARTESIAN_POINT ( 'NONE',  ( -130.5728709571500588, -24.75179208683297460, 8.640809912072082710 ) ) ;
#65250=CARTESIAN_POINT ( 'NONE',  ( 8.161054176536994831, -17.82452852192863091, -1.500000000000002220 ) ) ;
#65251=B_SPLINE_SURFACE_WITH_KNOTS ( 'NONE', 3, 3, ( 
 ( #58866, #65007, #80699, #73098 ),
 ( #96923, #10692, #95922, #3588 ),
 ( #25911, #4585, #26417, #89808 ),
 ( #42657, #73591, #57389, #66505 ),
 ( #34531, #18303, #35535, #50258 ),
 ( #12173, #20278, #4080, #96425 ),
 ( #35032, #81198, #51249, #82189 ) ),
 .UNSPECIFIED., .F., .F., .F.,
 ( 4, 3, 4 ),
 ( 4, 4 ),
 ( 0.0004766839783816928175, 0.1029713700210893867, 0.2054660560637970868 ),
 ( 0.6296541705118287036, 0.6309574163451897588 ),
 .UNSPECIFIED. ) ;
#65252=CARTESIAN_POINT ( 'NONE',  ( -49.87546937309745232, -25.30911630651809574, 4.600197623896191246 ) ) ;
#65253=ORIENTED_EDGE ( 'NONE', *, *, #59043, .T. ) ;
#65254=CARTESIAN_POINT ( 'NONE',  ( 4.075586527997184128, 21.15050231453075824, 11.49999999999998934 ) ) ;
#65257=CARTESIAN_POINT ( 'NONE',  ( -53.52287095715006870, -23.47596703998600631, 11.44779298504229104 ) ) ;
#65258=LINE ( 'NONE', #35287, #73111 ) ;
#65259=CARTESIAN_POINT ( 'NONE',  ( 22.59171682324826236, -3.780823453261925593, -1.500000000000002220 ) ) ;
#65261=ADVANCED_FACE ( 'NONE', ( #31812 ), #92040, .T. ) ;
#65264=CARTESIAN_POINT ( 'NONE',  ( -53.62368173164319529, -24.65952944569304250, 1.056160979905695463 ) ) ;
#65265=CARTESIAN_POINT ( 'NONE',  ( -18.95788008782500356, -6.583919088883305015, 11.49999999999999645 ) ) ;
#65267=CARTESIAN_POINT ( 'NONE',  ( -31.52287095715006160, -24.65952944569304606, 1.056160979905690134 ) ) ;
#65268=EDGE_CURVE ( 'NONE', #46589, #31325, #31214, .T. ) ;
#65269=CARTESIAN_POINT ( 'NONE',  ( -59.52287095715006160, -29.50248528299804818, 1.056150453629034924 ) ) ;
#65272=CARTESIAN_POINT ( 'NONE',  ( -18.60049703728633474, -6.982253431394513932, -1.500000000000002220 ) ) ;
#65275=CARTESIAN_POINT ( 'NONE',  ( -19.47062899137607772, 3.135797168518691169, -1.500000000000002220 ) ) ;
#65277=EDGE_CURVE ( 'NONE', #17423, #58197, #57843, .T. ) ;
#65279=AXIS2_PLACEMENT_3D ( 'NONE', #24536, #77805, #55505 ) ;
#65280=EDGE_CURVE ( 'NONE', #11225, #70943, #65036, .T. ) ;
#65282=CARTESIAN_POINT ( 'NONE',  ( -111.5228709571501042, -23.96127896941632685, -0.6493128931037972507 ) ) ;
#65283=CARTESIAN_POINT ( 'NONE',  ( 4.697267095454844998, -20.06606415395816967, 11.49999999999999645 ) ) ;
#65284=CARTESIAN_POINT ( 'NONE',  ( -49.52287095715006160, -29.50250786944525672, 11.44777988621624054 ) ) ;
#65285=CARTESIAN_POINT ( 'NONE',  ( -21.72567761722203628, 6.514095075961352954, 11.49999999999999645 ) ) ;
#65287=CARTESIAN_POINT ( 'NONE',  ( -69.34384048089543739, -25.12218957384244788, 6.239613635728673557 ) ) ;
#65288=CARTESIAN_POINT ( 'NONE',  ( -51.29483375901499898, -25.27820168282615754, 4.047861613338572084 ) ) ;
#65290=CARTESIAN_POINT ( 'NONE',  ( -27.65532027823855543, -24.61460113667579819, 8.251097176666958077 ) ) ;
#65291=CARTESIAN_POINT ( 'NONE',  ( -56.52287095715006870, -23.48786465467241058, 11.44779295918254824 ) ) ;
#65294=EDGE_CURVE ( 'NONE', #28213, #88368, #20246, .T. ) ;
#65296=CARTESIAN_POINT ( 'NONE',  ( 17.70901601935662839, 14.43836031950349152, -1.500000000000002220 ) ) ;
#65297=CARTESIAN_POINT ( 'NONE',  ( -105.5228709571500616, -24.99132157543084887, 2.256160258750667502 ) ) ;
#65299=CARTESIAN_POINT ( 'NONE',  ( -82.59968746745757073, -23.73791477778911840, 11.05961554403170766 ) ) ;
#65301=CARTESIAN_POINT ( 'NONE',  ( -5.125883829288005344, 21.89707322345674712, 11.49999999999999645 ) ) ;
#65303=CARTESIAN_POINT ( 'NONE',  ( -89.81226385320383088, -25.19340450609436743, 6.757884810855529167 ) ) ;
#65304=CARTESIAN_POINT ( 'NONE',  ( 18.29167757401336303, -12.14499471347784798, 11.49999999999998934 ) ) ;
#65306=EDGE_CURVE ( 'NONE', #28558, #29452, #41425, .T. ) ;
#65308=CARTESIAN_POINT ( 'NONE',  ( -112.5562042904833930, -24.64965694238575011, 8.947790433994189385 ) ) ;
#65309=VECTOR ( 'NONE', #44018, 1000.000000000000114 ) ;
#65310=VERTEX_POINT ( 'NONE', #58646 ) ;
#65311=CARTESIAN_POINT ( 'NONE',  ( -116.5228709571501042, -23.47593901973090524, -1.443836447538996426 ) ) ;
#65313=ORIENTED_EDGE ( 'NONE', *, *, #45606, .F. ) ;
#65314=CARTESIAN_POINT ( 'NONE',  ( -54.63855600440099636, -24.15620529776628089, 10.23563542870661180 ) ) ;
#65315=CARTESIAN_POINT ( 'NONE',  ( 12.01435098137705637, -16.61664908515649941, 11.49999999999998934 ) ) ;
#65316=VERTEX_POINT ( 'NONE', #82471 ) ;
#65317=ORIENTED_EDGE ( 'NONE', *, *, #51037, .T. ) ;
#65319=EDGE_LOOP ( 'NONE', ( #6846, #94731, #10792, #11717 ) ) ;
#65320=CARTESIAN_POINT ( 'NONE',  ( -80.60591430188112838, -25.13389835371019032, 7.097322268695329228 ) ) ;
#65321=CARTESIAN_POINT ( 'NONE',  ( 5.194767643164344584, 22.50260600399833422, 11.49999999999998934 ) ) ;
#65323=B_SPLINE_CURVE_WITH_KNOTS ( 'NONE', 3,
 ( #22866, #84783, #6163, #53353, #53851, #37115, #43742, #76655, #98503, #99000, #59971, #74676, #29494, #90407, #60477, #91393, #83783, #21870 ),
 .UNSPECIFIED., .F., .F.,
 ( 4, 2, 2, 2, 2, 2, 2, 2, 4 ),
 ( 0.000000000000000000, 0.1250000000000001388, 0.1875000000000000278, 0.2499999999999999445, 0.5000000000000001110, 0.7500000000000002220, 0.8125000000000001110, 0.8750000000000000000, 1.000000000000000000 ),
 .UNSPECIFIED. ) ;
#65324=CARTESIAN_POINT ( 'NONE',  ( -20.15914900662387055, -2.930279687489938389, -1.500000000000002220 ) ) ;
#65326=CARTESIAN_POINT ( 'NONE',  ( -29.67004714597209869, -23.41239500526456041, 11.44779303447556984 ) ) ;
#65327=ADVANCED_FACE ( 'NONE', ( #67267 ), #98690, .T. ) ;
#65328=CARTESIAN_POINT ( 'NONE',  ( -105.5608691116280511, -23.48783264082477018, -1.443836473390094355 ) ) ;
#65329=CARTESIAN_POINT ( 'NONE',  ( -57.58953762381671737, -23.48783264082478794, -1.443836473390068820 ) ) ;
#65330=ORIENTED_EDGE ( 'NONE', *, *, #4350, .T. ) ;
#65331=CARTESIAN_POINT ( 'NONE',  ( -27.68651082257922980, -25.21531658275831589, 2.274902402383796041 ) ) ;
#65332=CARTESIAN_POINT ( 'NONE',  ( -93.52287095715006160, -24.64965694238407323, 8.947790433994196491 ) ) ;
#65334=CARTESIAN_POINT ( 'NONE',  ( -15.76495264167062160, -13.51897010167481739, -1.500000000000002220 ) ) ;
#65335=ADVANCED_FACE ( 'NONE', ( #90092 ), #28817, .T. ) ;
#65336=ORIENTED_EDGE ( 'NONE', *, *, #65845, .F. ) ;
#65340=B_SPLINE_SURFACE_WITH_KNOTS ( 'NONE', 3, 1, ( 
 ( #55264, #62886 ),
 ( #16679, #25798 ),
 ( #86195, #9071 ),
 ( #56272, #85699 ),
 ( #47146, #78064 ),
 ( #1974, #94300 ),
 ( #47649, #24787 ),
 ( #8578, #48659 ),
 ( #39525, #17684 ),
 ( #55767, #79074 ),
 ( #9571, #71486 ),
 ( #22598, #92128 ),
 ( #83516, #68803 ),
 ( #23602, #38842 ),
 ( #69297, #77888 ) ),
 .UNSPECIFIED., .F., .F., .F.,
 ( 4, 1, 1, 1, 1, 1, 1, 1, 1, 1, 1, 1, 4 ),
 ( 2, 2 ),
 ( 0.000000000000000000, 0.07405842627338315998, 0.1488703523168777021, 0.2266676683691784822, 0.3077347594511126161, 0.3911572038059789591, 0.4739293555425539428, 0.5579277515150540268, 0.6449892900513599647, 0.7333640555176174081, 0.8210920421841580996, 0.9092872149973385554, 1.000000000000000000 ),
 ( 0.000000000000000000, 1.000000000000000000 ),
 .UNSPECIFIED. ) ;
#65341=CARTESIAN_POINT ( 'NONE',  ( -77.52287095715006160, -24.50216790748205042, 0.6166512839542531710 ) ) ;
#65342=CARTESIAN_POINT ( 'NONE',  ( -107.6228709571500701, -23.47593901973091235, -1.443836447538999312 ) ) ;
#65343=ORIENTED_EDGE ( 'NONE', *, *, #3223, .T. ) ;
#65344=VERTEX_POINT ( 'NONE', #66782 ) ;
#65345=CARTESIAN_POINT ( 'NONE',  ( -78.62287095715004170, -24.65952944569304606, 1.056160979905698349 ) ) ;
#65346=CARTESIAN_POINT ( 'NONE',  ( -116.6228709571501270, -24.35013146730204525, 9.818937971375104823 ) ) ;
#65347=CARTESIAN_POINT ( 'NONE',  ( -71.10442080388585850, -25.24515113135309718, 5.639839579979339490 ) ) ;
#65349=CARTESIAN_POINT ( 'NONE',  ( -9.261969182712835646, 20.05037652441878038, 11.49999999999999645 ) ) ;
#65350=ORIENTED_EDGE ( 'NONE', *, *, #18957, .F. ) ;
#65352=CARTESIAN_POINT ( 'NONE',  ( 18.79633983808273712, -12.56333175589740847, -1.500000000000002220 ) ) ;
#65353=DIRECTION ( 'NONE',  ( 3.773278334444167608E-23, -1.000000000000000000, 0.000000000000000000 ) ) ;
#65354=ORIENTED_EDGE ( 'NONE', *, *, #35263, .F. ) ;
#65358=LINE ( 'NONE', #80547, #55452 ) ;
#65359=ORIENTED_EDGE ( 'NONE', *, *, #10623, .T. ) ;
#65360=CARTESIAN_POINT ( 'NONE',  ( -19.38594737788604405, 8.525550480899875438, 11.49999999999998934 ) ) ;
#65361=CARTESIAN_POINT ( 'NONE',  ( -125.6228709571500559, -24.62226745350437795, 0.9660975649728152925 ) ) ;
#65362=CARTESIAN_POINT ( 'NONE',  ( -40.58094919657983723, -25.29362508255670150, 5.541655676671355835 ) ) ;
#65363=CARTESIAN_POINT ( 'NONE',  ( 10.78255534502030777, 19.45608938089507234, -1.500000000000002220 ) ) ;
#65365=EDGE_LOOP ( 'NONE', ( #26742, #51276, #29063, #57583 ) ) ;
#65366=LINE ( 'NONE', #33887, #88681 ) ;
#65368=CARTESIAN_POINT ( 'NONE',  ( -36.66656757783551512, -23.48786465467240347, 11.44779295918255180 ) ) ;
#65371=CARTESIAN_POINT ( 'NONE',  ( -16.58133674543539371, -10.29093563426468450, 11.49999999999998934 ) ) ;
#65373=CARTESIAN_POINT ( 'NONE',  ( 21.23773461148298836, -3.020459416520930862, -1.500000000000002220 ) ) ;
#65374=CARTESIAN_POINT ( 'NONE',  ( -26.47871760004291630, -24.57999593927708304, 2.074685142752674238 ) ) ;
#65376=CARTESIAN_POINT ( 'NONE',  ( -77.50432408278001617, -24.34968618360934300, 0.1864209137778811143 ) ) ;
#65377=CARTESIAN_POINT ( 'NONE',  ( 22.46337926046256328, 3.617889471270266277, -1.500000000000002220 ) ) ;
#65379=EDGE_CURVE ( 'NONE', #50584, #82905, #83142, .T. ) ;
#65380=CARTESIAN_POINT ( 'NONE',  ( -98.62355863167962866, -24.65952944569305316, 1.056160979905700570 ) ) ;
#65381=CARTESIAN_POINT ( 'NONE',  ( -128.5228709571500758, -23.47593901973090524, -1.443836447538996204 ) ) ;
#65382=CARTESIAN_POINT ( 'NONE',  ( -8.676013072486071565, -17.92234406281952275, 11.49999999999999645 ) ) ;
#65383=CARTESIAN_POINT ( 'NONE',  ( -101.6228709571500559, -23.48786465467242479, 11.44779295918254114 ) ) ;
#65384=ADVANCED_FACE ( 'NONE', ( #90585 ), #29185, .T. ) ;
#65387=CARTESIAN_POINT ( 'NONE',  ( -39.60068811824800150, -23.96169478059713143, 10.65365249895718769 ) ) ;
#65388=B_SPLINE_CURVE_WITH_KNOTS ( 'NONE', 3,
 ( #81159, #73551, #33480, #4043 ),
 .UNSPECIFIED., .F., .F.,
 ( 4, 4 ),
 ( 0.000000000000000000, 1.000000000000000000 ),
 .UNSPECIFIED. ) ;
#65389=CARTESIAN_POINT ( 'NONE',  ( -48.53564735683374209, -24.51314013834315375, 0.6176544820404137326 ) ) ;
#65390=ORIENTED_EDGE ( 'NONE', *, *, #88971, .F. ) ;
#65392=CARTESIAN_POINT ( 'NONE',  ( -77.52287095715004739, -23.73907113216989728, -1.053371485793253903 ) ) ;
#65394=CARTESIAN_POINT ( 'NONE',  ( 21.69746526873944958, -0.4026533170205861545, -1.500000000000002220 ) ) ;
#65395=CARTESIAN_POINT ( 'NONE',  ( -51.76873150024551506, -25.17952130149804191, 6.819150868768721452 ) ) ;
#65396=CARTESIAN_POINT ( 'NONE',  ( -13.92019785312828972, -13.74635529968554515, -1.500000000000002220 ) ) ;
#65397=EDGE_CURVE ( 'NONE', #21, #85607, #62144, .T. ) ;
#65402=CARTESIAN_POINT ( 'NONE',  ( -19.81292649638395531, 4.959676026661640869, 11.49999999999999645 ) ) ;
#65403=CARTESIAN_POINT ( 'NONE',  ( -41.62287095715006302, -29.50250243563736774, 8.947779886222148704 ) ) ;
#65404=CARTESIAN_POINT ( 'NONE',  ( -60.24005924445285842, -25.32056586294729783, 4.734103931585309510 ) ) ;
#65405=VERTEX_POINT ( 'NONE', #24560 ) ;
#65407=FACE_OUTER_BOUND ( 'NONE', #82975, .T. ) ;
#65408=CARTESIAN_POINT ( 'NONE',  ( -125.5895376238167245, -23.48786465467241769, 11.44779295918253403 ) ) ;
#65409=( BOUNDED_SURFACE ( )  B_SPLINE_SURFACE ( 3, 1, ( 
 ( #27498, #67069 ),
 ( #65581, #80783 ),
 ( #57461, #87891 ),
 ( #12245, #74164 ) ),
 .UNSPECIFIED., .F., .F., .T. ) 
 B_SPLINE_SURFACE_WITH_KNOTS ( ( 4, 4 ),
 ( 2, 2 ),
 ( 0.000000000000000000, 1.000000000000000000 ),
 ( 0.000000000000000000, 1.000000000000000000 ),
 .UNSPECIFIED. ) 
 GEOMETRIC_REPRESENTATION_ITEM ( )  RATIONAL_B_SPLINE_SURFACE ( (
 ( 1.000000000000000000, 1.000000000000000000),
 ( 0.3333333333333333703, 0.3333333333333333703),
 ( 0.3333333333333333703, 0.3333333333333333703),
 ( 1.000000000000000000, 1.000000000000000000) ) ) 
 REPRESENTATION_ITEM ( '' )  SURFACE ( )  );
#65410=B_SPLINE_CURVE_WITH_KNOTS ( 'NONE', 3,
 ( #63665, #94587, #79357, #25068 ),
 .UNSPECIFIED., .F., .F.,
 ( 4, 4 ),
 ( 5.511242692161060920E-09, 0.0003958033267307038716 ),
 .UNSPECIFIED. ) ;
#65413=ORIENTED_EDGE ( 'NONE', *, *, #34721, .T. ) ;
#65414=CARTESIAN_POINT ( 'NONE',  ( -128.5228709571500758, -29.50250243563736774, 8.947779886222132717 ) ) ;
#65415=CARTESIAN_POINT ( 'NONE',  ( -20.69623851537618364, -9.862649113751288610, 11.49999999999999645 ) ) ;
#65416=CARTESIAN_POINT ( 'NONE',  ( 10.97283692364161922, -19.94330716608196852, 11.49999999999998934 ) ) ;
#65417=CARTESIAN_POINT ( 'NONE',  ( -70.52865987952087323, -25.04472902735052031, 7.555535287402955547 ) ) ;
#65418=VECTOR ( 'NONE', #14655, 1000.000000000000114 ) ;
#65420=CARTESIAN_POINT ( 'NONE',  ( -90.56379385379925395, -23.48783264082477018, -1.443836473390091690 ) ) ;
#65422=CARTESIAN_POINT ( 'NONE',  ( -89.52287095715003318, -23.48783264083374789, -1.443836473376144180 ) ) ;
#65423=CARTESIAN_POINT ( 'NONE',  ( 11.25260618158950621, 18.78031238747207610, -1.500000000000002220 ) ) ;
#65424=LINE ( 'NONE', #58291, #41395 ) ;
#65427=CARTESIAN_POINT ( 'NONE',  ( -58.54270549319968353, -24.34968618360933945, 0.1864209137778795045 ) ) ;
#65429=CARTESIAN_POINT ( 'NONE',  ( -12.12210191164509965, 16.44476101713275185, 11.49999999999998934 ) ) ;
#65432=ORIENTED_EDGE ( 'NONE', *, *, #96458, .F. ) ;
#65433=CARTESIAN_POINT ( 'NONE',  ( -14.43837761634077310, -17.93274050997184332, 11.49999999999998934 ) ) ;
#65435=CARTESIAN_POINT ( 'NONE',  ( -20.16912494768211417, -0.3064379698199363733, -1.500000000000002220 ) ) ;
#65437=CARTESIAN_POINT ( 'NONE',  ( -67.62287095715005592, -23.48786465467241058, 11.44779295918254647 ) ) ;
#65439=CARTESIAN_POINT ( 'NONE',  ( -95.50652094920334889, -24.63355581998386157, 0.9682620441943944334 ) ) ;
#65441=CARTESIAN_POINT ( 'NONE',  ( -19.64189229742525455, -8.423329616690555355, 11.49999999999999645 ) ) ;
#65445=CARTESIAN_POINT ( 'NONE',  ( 22.02009960291501045, 3.200778107580485532, 11.49999999999998934 ) ) ;
#65446=CARTESIAN_POINT ( 'NONE',  ( -18.79711486612840332, 8.613068827758688428, 11.49999999999998934 ) ) ;
#65447=EDGE_CURVE ( 'NONE', #40883, #95766, #727, .T. ) ;
#65448=ORIENTED_EDGE ( 'NONE', *, *, #31209, .T. ) ;
#65449=ADVANCED_FACE ( 'NONE', ( #39290 ), #23550, .T. ) ;
#65451=VERTEX_POINT ( 'NONE', #54036 ) ;
#65453=ORIENTED_EDGE ( 'NONE', *, *, #96315, .T. ) ;
#65454=AXIS2_PLACEMENT_3D ( 'NONE', #74822, #66249, #44896 ) ;
#65455=CARTESIAN_POINT ( 'NONE',  ( -50.32469610480872291, -25.27517877801826884, 2.834264043007450162 ) ) ;
#65456=CARTESIAN_POINT ( 'NONE',  ( -7.180602670292889123, -19.69607742855361465, -1.500000000000002220 ) ) ;
#65457=CARTESIAN_POINT ( 'NONE',  ( -15.13543854793762300, 15.80457324685279374, 11.49999999999999645 ) ) ;
#65458=CARTESIAN_POINT ( 'NONE',  ( -26.43901205547898670, -24.77993617750158606, 6.777242332140119174 ) ) ;
#65459=CARTESIAN_POINT ( 'NONE',  ( 8.356338879324495039, -20.90460381316865934, 11.49999999999998934 ) ) ;
#65460=B_SPLINE_CURVE_WITH_KNOTS ( 'NONE', 3,
 ( #5352, #52032, #45419, #61152 ),
 .UNSPECIFIED., .F., .F.,
 ( 4, 4 ),
 ( 0.000000000000000000, 9.999999999999592548E-05 ),
 .UNSPECIFIED. ) ;
#65461=CARTESIAN_POINT ( 'NONE',  ( 0.8316226063609513108, 20.92010288561657205, -1.500000000000002220 ) ) ;
#65465=CARTESIAN_POINT ( 'NONE',  ( -70.62287095715007013, -23.47596703998600631, 11.44779298504227505 ) ) ;
#65466=ORIENTED_EDGE ( 'NONE', *, *, #72142, .T. ) ;
#65467=ORIENTED_EDGE ( 'NONE', *, *, #73811, .F. ) ;
#65470=ORIENTED_EDGE ( 'NONE', *, *, #38995, .T. ) ;
#65471=CARTESIAN_POINT ( 'NONE',  ( 10.13398631766115443, 18.95262098133242290, -1.500000000000002220 ) ) ;
#65472=ORIENTED_EDGE ( 'NONE', *, *, #100331, .F. ) ;
#65474=CARTESIAN_POINT ( 'NONE',  ( 14.35337761433406811, 15.45585641580067104, -1.500000000000002220 ) ) ;
#65475=CARTESIAN_POINT ( 'NONE',  ( -52.62287095715007013, -24.33927499327854704, 9.819080762295820719 ) ) ;
#65476=FACE_OUTER_BOUND ( 'NONE', #38366, .T. ) ;
#65478=PLANE ( 'NONE',  #96143 ) ;
#65479=CARTESIAN_POINT ( 'NONE',  ( -129.5218485930514873, -24.51419770103158413, 9.386484678747176957 ) ) ;
#65480=CARTESIAN_POINT ( 'NONE',  ( 14.91618686576236108, -16.25093855066790738, -1.500000000000002220 ) ) ;
#65481=VERTEX_POINT ( 'NONE', #47415 ) ;
#65482=CARTESIAN_POINT ( 'NONE',  ( -116.5175178794913649, -24.34968618360935366, 0.1864209137779019587 ) ) ;
#65483=AXIS2_PLACEMENT_3D ( 'NONE', #65052, #33574, #57432 ) ;
#65484=CARTESIAN_POINT ( 'NONE',  ( -111.6228709571500701, -23.96177878511308634, 10.65340807706329862 ) ) ;
#65485=CARTESIAN_POINT ( 'NONE',  ( -78.62287095715005592, -23.73934037231757799, 11.05740245334328442 ) ) ;
#65487=CARTESIAN_POINT ( 'NONE',  ( -62.53524634668898585, -24.66019654487199730, 8.947790411086124607 ) ) ;
#65489=CARTESIAN_POINT ( 'NONE',  ( -121.6228709571500417, -29.50250243563736774, 8.947779886222134493 ) ) ;
#65491=CARTESIAN_POINT ( 'NONE',  ( -5.188002292566340934, -20.72503599944539587, -1.500000000000002220 ) ) ;
#65492=CARTESIAN_POINT ( 'NONE',  ( -81.52287095715010423, -23.47593901973090524, -1.443836447538996648 ) ) ;
#65493=CARTESIAN_POINT ( 'NONE',  ( -48.85554520786481447, -25.25978491487771649, 3.590542621692356384 ) ) ;
#65495=FACE_OUTER_BOUND ( 'NONE', #59523, .T. ) ;
#65496=CARTESIAN_POINT ( 'NONE',  ( 22.48748499206561746, 2.281147167042596013, -1.500000000000002220 ) ) ;
#65497=LINE ( 'NONE', #96419, #40972 ) ;
#65500=CARTESIAN_POINT ( 'NONE',  ( -79.49885629545516963, -24.65952944569304606, 1.056160979905700126 ) ) ;
#65501=CARTESIAN_POINT ( 'NONE',  ( -14.12090166725071327, 13.77431136191591143, 11.49999999999999645 ) ) ;
#65502=CARTESIAN_POINT ( 'NONE',  ( -82.62287095715007013, -24.50321055353805377, 9.387540953477531147 ) ) ;
#65504=CARTESIAN_POINT ( 'NONE',  ( -104.6228709571500559, -29.50250243563736774, 8.947779886222138046 ) ) ;
#65505=ORIENTED_EDGE ( 'NONE', *, *, #64466, .F. ) ;
#65507=CARTESIAN_POINT ( 'NONE',  ( -29.81116077451118329, -25.26026984619284121, 4.841835660607406666 ) ) ;
#65509=CARTESIAN_POINT ( 'NONE',  ( -47.52287095715006160, -29.50248528299804818, 1.056150453629033370 ) ) ;
#65510=CARTESIAN_POINT ( 'NONE',  ( -21.01067979154616694, 5.129389437380057259, -1.500000000000002220 ) ) ;
#65511=CARTESIAN_POINT ( 'NONE',  ( -126.6228709571500559, -24.64965695001469825, 8.947790433994173398 ) ) ;
#65512=CARTESIAN_POINT ( 'NONE',  ( -2.960655606634402748, -19.13016773636607581, -1.500000000000002220 ) ) ;
#65513=ADVANCED_FACE ( 'NONE', ( #84961 ), #8844, .F. ) ;
#65515=CARTESIAN_POINT ( 'NONE',  ( -118.5228709571500758, -24.64965694238408034, 8.947790433994191162 ) ) ;
#65516=CARTESIAN_POINT ( 'NONE',  ( 6.953341435731974940, 18.52374150113109152, -1.500000000000002220 ) ) ;
#65519=CARTESIAN_POINT ( 'NONE',  ( 13.55758662847591900, -15.04642845256218031, 11.49999999999999645 ) ) ;
#65523=CARTESIAN_POINT ( 'NONE',  ( -67.52287095715009002, -24.35013146730203815, 9.818937971375095941 ) ) ;
#65524=FACE_OUTER_BOUND ( 'NONE', #74517, .T. ) ;
#65526=CARTESIAN_POINT ( 'NONE',  ( -69.55126625704997423, -25.15208592601422311, 3.076695591939294427 ) ) ;
#65527=CARTESIAN_POINT ( 'NONE',  ( -44.52287095715006160, -24.64965694238575011, 8.947790433994205372 ) ) ;
#65528=CARTESIAN_POINT ( 'NONE',  ( -71.62287095715005592, -23.94994826722565762, -0.6494450866342720285 ) ) ;
#65529=CARTESIAN_POINT ( 'NONE',  ( -10.14125802585430947, 17.27231531754821603, -1.500000000000002220 ) ) ;
#65530=ADVANCED_FACE ( 'NONE', ( #62647 ), #46408, .T. ) ;
#65533=CARTESIAN_POINT ( 'NONE',  ( -90.58953762381672448, -23.47596703998600631, 11.44779298504227683 ) ) ;
#65534=DIRECTION ( 'NONE',  ( 0.000000000000000000, -0.9999999999976377785, -2.173523156925979128E-06 ) ) ;
#65535=DIRECTION ( 'NONE',  ( -3.773278334453079030E-23, 0.9999999999976377785, 2.173523156925979128E-06 ) ) ;
#65536=B_SPLINE_CURVE_WITH_KNOTS ( 'NONE', 3,
 ( #82254, #61930, #67546, #59939, #6629, #22831 ),
 .UNSPECIFIED., .F., .F.,
 ( 4, 2, 4 ),
 ( 0.000000000000000000, 0.001380901958385382473, 0.002761803916770764946 ),
 .UNSPECIFIED. ) ;
#65537=DIRECTION ( 'NONE',  ( 0.000000000000000000, 2.173523156925980399E-06, -0.9999999999976378895 ) ) ;
#65538=CARTESIAN_POINT ( 'NONE',  ( -45.52287095715006160, -25.00158670708908915, 2.256160236439166411 ) ) ;
#65539=VECTOR ( 'NONE', #48277, 1000.000000000000114 ) ;
#65541=CARTESIAN_POINT ( 'NONE',  ( -49.26828308126997769, -25.12100811749006724, 7.112893600995336740 ) ) ;
#65543=CARTESIAN_POINT ( 'NONE',  ( 5.487062353440709472, 19.58251264919930534, 11.49999999999998934 ) ) ;
#65544=EDGE_LOOP ( 'NONE', ( #45500, #30170, #6739, #1704 ) ) ;
#65546=CARTESIAN_POINT ( 'NONE',  ( -22.92702450682246251, 0.3551139841105944162, 11.49999999999998934 ) ) ;
#65549=VERTEX_POINT ( 'NONE', #61155 ) ;
#65550=CARTESIAN_POINT ( 'NONE',  ( -96.52287095715006160, -29.50250243563736774, 8.947779886222138046 ) ) ;
#65552=EDGE_CURVE ( 'NONE', #72410, #94726, #92842, .T. ) ;
#65553=B_SPLINE_CURVE_WITH_KNOTS ( 'NONE', 3,
 ( #44877, #75799, #73813, #74803, #37257, #29633 ),
 .UNSPECIFIED., .F., .F.,
 ( 4, 2, 4 ),
 ( 0.000000000000000000, 0.001380764517854760846, 0.002761529035709521691 ),
 .UNSPECIFIED. ) ;
#65555=CARTESIAN_POINT ( 'NONE',  ( -6.524719417830534773, 20.15472526627327454, 11.49999999999999645 ) ) ;
#65556=CARTESIAN_POINT ( 'NONE',  ( 17.13038851031509680, -14.05419017248541813, 11.49999999999998934 ) ) ;
#65558=CARTESIAN_POINT ( 'NONE',  ( 15.34425395324244867, 13.73259486114767114, -1.500000000000002220 ) ) ;
#65559=ORIENTED_EDGE ( 'NONE', *, *, #29385, .F. ) ;
#65560=CARTESIAN_POINT ( 'NONE',  ( -41.56943525746097379, -23.48783264082477729, -1.443836473390076147 ) ) ;
#65561=ORIENTED_EDGE ( 'NONE', *, *, #35493, .T. ) ;
#65562=CARTESIAN_POINT ( 'NONE',  ( -54.63855744824223137, -24.15543982623906416, -0.2315651400026691176 ) ) ;
#65564=CARTESIAN_POINT ( 'NONE',  ( -50.52287095715006160, -24.82576562948880294, 8.398263436605674315 ) ) ;
#65568=CARTESIAN_POINT ( 'NONE',  ( -116.6228709571500417, -23.95044443724992433, 10.65354141964649237 ) ) ;
#65569=FACE_OUTER_BOUND ( 'NONE', #42603, .T. ) ;
#65570=DIRECTION ( 'NONE',  ( -3.773278334453080206E-23, 0.9999999999976377785, 2.173523156925979975E-06 ) ) ;
#65571=CARTESIAN_POINT ( 'NONE',  ( 17.59156710592704442, 10.99281682905060897, -1.500000000000002220 ) ) ;
#65572=CARTESIAN_POINT ( 'NONE',  ( 2.995010171738120786, 21.53247193037183038, 11.49999999999999645 ) ) ;
#65573=ORIENTED_EDGE ( 'NONE', *, *, #63923, .T. ) ;
#65574=CARTESIAN_POINT ( 'NONE',  ( -62.62287095715004881, -24.65952944569304606, 1.056160979905693909 ) ) ;
#65575=CARTESIAN_POINT ( 'NONE',  ( -37.52287095715006870, -24.65952944569304250, 1.056160979905691910 ) ) ;
#65576=CARTESIAN_POINT ( 'NONE',  ( 12.67250375155129127, 18.46511205475877304, 11.49999999999998934 ) ) ;
#65577=CARTESIAN_POINT ( 'NONE',  ( -33.52287095715006160, -24.64965694238574656, 8.947790433994207149 ) ) ;
#65579=ORIENTED_EDGE ( 'NONE', *, *, #13785, .F. ) ;
#65580=CARTESIAN_POINT ( 'NONE',  ( -31.62287095715003815, -24.35013146730203459, 9.818937971375119034 ) ) ;
#65581=CARTESIAN_POINT ( 'NONE',  ( -119.4728709548940628, -25.40673988423724694, 2.000950539785692150 ) ) ;
#65582=VECTOR ( 'NONE', #14908, 1000.000000000000114 ) ;
#65583=VERTEX_POINT ( 'NONE', #88479 ) ;
#65585=CARTESIAN_POINT ( 'NONE',  ( -103.6228709571500133, -23.72747288104441665, -1.053458166803660445 ) ) ;
#65588=CARTESIAN_POINT ( 'NONE',  ( 21.11169859150035677, 2.410084449224629832, -1.500000000000002220 ) ) ;
#65590=CARTESIAN_POINT ( 'NONE',  ( -88.51440607272326133, -23.96119346886880308, -0.6495511937832096905 ) ) ;
#65591=CARTESIAN_POINT ( 'NONE',  ( 19.20967809413044236, -10.42350525531561978, 11.49999999999998934 ) ) ;
#65592=PLANE ( 'NONE',  #82168 ) ;
#65593=CARTESIAN_POINT ( 'NONE',  ( -22.63693132222386950, 1.387278323242118416, 11.49999999999998934 ) ) ;
#65594=CARTESIAN_POINT ( 'NONE',  ( -40.65892442973913745, -25.28892425236737296, 3.308409971807110050 ) ) ;
#65596=CARTESIAN_POINT ( 'NONE',  ( 17.39636294008568740, -13.23181597624684791, -1.500000000000002220 ) ) ;
#65599=CARTESIAN_POINT ( 'NONE',  ( -65.62287095715005592, -24.52232992886362695, 0.6492154411906108091 ) ) ;
#65600=CARTESIAN_POINT ( 'NONE',  ( -126.6228709571500843, -24.65952944569305316, 1.056160979905707675 ) ) ;
#65602=CARTESIAN_POINT ( 'NONE',  ( -90.62287095715004170, -25.00158670708908915, 2.256160236439166411 ) ) ;
#65606=CARTESIAN_POINT ( 'NONE',  ( 13.48273455363431772, -16.43370779934446801, -1.500000000000002220 ) ) ;
#65608=CARTESIAN_POINT ( 'NONE',  ( -26.12582186233688830, -24.75186408905701541, 4.293464003132087647 ) ) ;
#65609=VECTOR ( 'NONE', #92327, 1000.000000000000114 ) ;
#65610=LINE ( 'NONE', #36131, #16235 ) ;
#65611=DIRECTION ( 'NONE',  ( 3.773278334444167020E-23, -1.000000000000000000, 0.000000000000000000 ) ) ;
#65612=B_SPLINE_CURVE_WITH_KNOTS ( 'NONE', 3,
 ( #54699, #76012, #69914, #37469 ),
 .UNSPECIFIED., .F., .F.,
 ( 4, 4 ),
 ( 1.486098242880303625E-05, 0.002476302731154660791 ),
 .UNSPECIFIED. ) ;
#65613=CARTESIAN_POINT ( 'NONE',  ( -117.5555597079124936, -23.96169478059714564, 10.65365249895717170 ) ) ;
#65614=ORIENTED_EDGE ( 'NONE', *, *, #94734, .T. ) ;
#65615=CARTESIAN_POINT ( 'NONE',  ( 15.80261042061247068, 11.49252619723154112, 11.49999999999999645 ) ) ;
#65617=EDGE_CURVE ( 'NONE', #6691, #51543, #38400, .T. ) ;
#65618=LINE ( 'NONE', #74689, #77158 ) ;
#65619=ORIENTED_EDGE ( 'NONE', *, *, #41828, .F. ) ;
#65621=LINE ( 'NONE', #96538, #14987 ) ;
#65622=CARTESIAN_POINT ( 'NONE',  ( -99.42228033019944178, -25.31551726817962944, 5.054791656742963823 ) ) ;
#65623=CARTESIAN_POINT ( 'NONE',  ( -94.52287095715006160, -29.50250243563736774, 8.947779886222139822 ) ) ;
#65625=CARTESIAN_POINT ( 'NONE',  ( -17.62575346185542102, 8.740161020289619387, 11.49999999999998934 ) ) ;
#65626=ORIENTED_EDGE ( 'NONE', *, *, #45923, .T. ) ;
#65627=EDGE_CURVE ( 'NONE', #2525, #86407, #841, .T. ) ;
#65628=DIRECTION ( 'NONE',  ( -3.773278334453079618E-23, 0.9999999999976377785, 2.173523156925979975E-06 ) ) ;
#65630=ADVANCED_FACE ( 'NONE', ( #9842 ), #79850, .F. ) ;
#65633=CARTESIAN_POINT ( 'NONE',  ( -74.52287095715011844, -24.51283580621364422, 0.6167428607019772580 ) ) ;
#65634=FACE_OUTER_BOUND ( 'NONE', #51985, .T. ) ;
#65636=CARTESIAN_POINT ( 'NONE',  ( -97.59978409505167463, -23.48786465467241413, 11.44779295918254469 ) ) ;
#65639=CARTESIAN_POINT ( 'NONE',  ( -114.5584140531362607, -23.48786465467241413, 11.44779295918253581 ) ) ;
#65640=CARTESIAN_POINT ( 'NONE',  ( 15.91301918423788919, -12.03417825965012433, 11.49999999999998934 ) ) ;
#65641=B_SPLINE_CURVE_WITH_KNOTS ( 'NONE', 3,
 ( #90511, #6271, #92498, #28617 ),
 .UNSPECIFIED., .F., .F.,
 ( 4, 4 ),
 ( 0.000000000000000000, 9.999999999998897304E-05 ),
 .UNSPECIFIED. ) ;
#65642=EDGE_CURVE ( 'NONE', #81135, #87028, #63656, .T. ) ;
#65643=CARTESIAN_POINT ( 'NONE',  ( -0.03818598950967933697, -22.55565235769328680, 8.432995269277139272 ) ) ;
#65644=CARTESIAN_POINT ( 'NONE',  ( 14.98761344906185577, -13.09354923471379983, -1.500000000000002220 ) ) ;
#65646=B_SPLINE_CURVE_WITH_KNOTS ( 'NONE', 3,
 ( #6454, #99291, #36405, #51638 ),
 .UNSPECIFIED., .F., .F.,
 ( 4, 4 ),
 ( 0.000000000000000000, 9.999999999999592548E-05 ),
 .UNSPECIFIED. ) ;
#65648=B_SPLINE_CURVE_WITH_KNOTS ( 'NONE', 3,
 ( #70389, #33317, #87108, #79996 ),
 .UNSPECIFIED., .F., .F.,
 ( 4, 4 ),
 ( 0.000000000000000000, 9.999999999998900014E-05 ),
 .UNSPECIFIED. ) ;
#65652=CARTESIAN_POINT ( 'NONE',  ( -18.78340662496949776, 8.880393494302802893, 11.49999999999999645 ) ) ;
#65655=CARTESIAN_POINT ( 'NONE',  ( -6.082769120682566921, -21.99330073093985405, 11.49999999999999645 ) ) ;
#65656=EDGE_LOOP ( 'NONE', ( #23995, #68424, #79528, #14886 ) ) ;
#65658=CARTESIAN_POINT ( 'NONE',  ( -103.6228709571500559, -29.50250243563736774, 8.947779886222138046 ) ) ;
#65659=EDGE_LOOP ( 'NONE', ( #10806, #88498, #30233, #52564 ) ) ;
#65660=CARTESIAN_POINT ( 'NONE',  ( 9.769481717609929561, -17.74358427669893956, -1.500000000000002220 ) ) ;
#65661=EDGE_CURVE ( 'NONE', #9193, #14515, #97704, .T. ) ;
#65662=CARTESIAN_POINT ( 'NONE',  ( -108.6228709571500559, -24.64965695001468404, 8.947790433994176951 ) ) ;
#65664=CARTESIAN_POINT ( 'NONE',  ( -115.6228709571500559, -23.47593901973091235, -1.443836447538997536 ) ) ;
#65665=ORIENTED_EDGE ( 'NONE', *, *, #464, .T. ) ;
#65666=CARTESIAN_POINT ( 'NONE',  ( -80.29437483463682668, -25.31554926095677160, 4.970974304119136988 ) ) ;
#65668=CARTESIAN_POINT ( 'NONE',  ( -30.47287095715007510, -23.47596699454220470, 11.42688508591989560 ) ) ;
#65669=CARTESIAN_POINT ( 'NONE',  ( 18.34943919012036773, 8.063251210807163005, -1.500000000000002220 ) ) ;
#65670=CARTESIAN_POINT ( 'NONE',  ( -0.5131542516139314669, 21.03015271272555253, 11.49999999999999645 ) ) ;
#65673=CARTESIAN_POINT ( 'NONE',  ( 15.63414672909509839, 15.54323407889855879, -1.500000000000002220 ) ) ;
#65676=CARTESIAN_POINT ( 'NONE',  ( -46.62287095715004881, -23.47593901973091235, -1.443836447539009749 ) ) ;
#65677=EDGE_CURVE ( 'NONE', #84515, #18736, #99055, .T. ) ;
#65678=CARTESIAN_POINT ( 'NONE',  ( -47.55620429048338593, -24.65952944569304606, 1.056160979905693686 ) ) ;
#65679=CARTESIAN_POINT ( 'NONE',  ( -50.36897396760109302, -25.18440102080580445, 3.294677851422761261 ) ) ;
#65681=CARTESIAN_POINT ( 'NONE',  ( -31.62287095715005236, -24.65952944569304250, 1.056160979905689690 ) ) ;
#65683=VERTEX_POINT ( 'NONE', #37178 ) ;
#65687=CARTESIAN_POINT ( 'NONE',  ( 20.53815866822273861, -0.6333348845813139283, -1.500000000000002220 ) ) ;
#65693=CARTESIAN_POINT ( 'NONE',  ( -12.45998644600372884, -18.51849504856558681, -1.500000000000002220 ) ) ;
#65694=AXIS2_PLACEMENT_3D ( 'NONE', #46810, #78729, #23437 ) ;
#65695=CARTESIAN_POINT ( 'NONE',  ( -0.07188169300783603388, -22.11943499646449141, 0.5637492489085904612 ) ) ;
#65696=CARTESIAN_POINT ( 'NONE',  ( -31.58953762381672092, -23.48783264082477729, -1.443836473390074149 ) ) ;
#65697=VERTEX_POINT ( 'NONE', #12830 ) ;
#65698=CARTESIAN_POINT ( 'NONE',  ( -32.62287095715004881, -23.72773821059535848, 11.05748984161097503 ) ) ;
#65699=CARTESIAN_POINT ( 'NONE',  ( -51.57158818203188844, -25.29445700113289419, 4.475956743242817559 ) ) ;
#65700=CARTESIAN_POINT ( 'NONE',  ( 20.25184064777635484, 4.944226511633750043, 11.49999999999998934 ) ) ;
#65701=VERTEX_POINT ( 'NONE', #97575 ) ;
#65702=DIRECTION ( 'NONE',  ( 0.000000000000000000, -0.9999999999976377785, -2.173523156925979975E-06 ) ) ;
#65703=ORIENTED_EDGE ( 'NONE', *, *, #86319, .T. ) ;
#65704=EDGE_CURVE ( 'NONE', #88376, #71422, #78280, .T. ) ;
#65706=CARTESIAN_POINT ( 'NONE',  ( -68.93918693012690824, -25.25935051156955780, 6.184868435727651992 ) ) ;
#65707=CARTESIAN_POINT ( 'NONE',  ( -18.71117167593497399, 9.704403692310313190, -1.500000000000002220 ) ) ;
#65708=ORIENTED_EDGE ( 'NONE', *, *, #15186, .F. ) ;
#65711=DIRECTION ( 'NONE',  ( 0.000000000000000000, -2.173523156925979552E-06, 0.9999999999976378895 ) ) ;
#65714=DIRECTION ( 'NONE',  ( 0.000000000000000000, -0.9999999999976377785, -2.173523156925979975E-06 ) ) ;
#65715=CARTESIAN_POINT ( 'NONE',  ( -6.994818212361641585, 20.52682044044541598, -1.500000000000002220 ) ) ;
#65716=CARTESIAN_POINT ( 'NONE',  ( -81.48149462243461016, -25.12224216488500517, 6.293943252966847091 ) ) ;
#65717=CARTESIAN_POINT ( 'NONE',  ( -4.073883676365832152, 21.86232641878667593, 11.49999999999999645 ) ) ;
#65718=ORIENTED_EDGE ( 'NONE', *, *, #55288, .T. ) ;
#65719=CARTESIAN_POINT ( 'NONE',  ( -51.39979512284951824, -25.24728839109623024, 5.729492026579687369 ) ) ;
#65721=CARTESIAN_POINT ( 'NONE',  ( -106.5228709571500758, -23.95044443724991723, 10.65354141964648704 ) ) ;
#65722=VERTEX_POINT ( 'NONE', #43799 ) ;
#65723=EDGE_CURVE ( 'NONE', #47263, #40585, #37138, .T. ) ;
#65724=EDGE_CURVE ( 'NONE', #94858, #67184, #28701, .T. ) ;
#65725=CARTESIAN_POINT ( 'NONE',  ( -104.6228709571500559, -23.47596703998600631, 11.44779298504227860 ) ) ;
#65727=EDGE_LOOP ( 'NONE', ( #10418, #66470, #78744, #59926 ) ) ;
#65728=CARTESIAN_POINT ( 'NONE',  ( -10.30982817980527777, -21.98926139291979709, -1.497999999999531928 ) ) ;
#65729=LINE ( 'NONE', #98133, #30801 ) ;
#65733=CARTESIAN_POINT ( 'NONE',  ( -39.52287095715006870, -23.48786465467241058, 11.44779295918255180 ) ) ;
#65734=CARTESIAN_POINT ( 'NONE',  ( 12.99221220249228281, -18.32192329980629708, -1.500000000000002220 ) ) ;
#65738=CARTESIAN_POINT ( 'NONE',  ( -101.5910247417354100, -24.15620529776628800, 10.23563542870660292 ) ) ;
#65740=CARTESIAN_POINT ( 'NONE',  ( -49.52287095715007581, -23.47593901973090169, -1.443836447538997092 ) ) ;
#65741=CARTESIAN_POINT ( 'NONE',  ( -30.57951640616625255, -25.14064729901805251, 2.712351064733618422 ) ) ;
#65742=CARTESIAN_POINT ( 'NONE',  ( 17.63768857353127828, -8.544740250177758512, 11.49999999999998934 ) ) ;
#65743=CARTESIAN_POINT ( 'NONE',  ( -49.70995324199571996, -25.30398808162055957, 4.467198061186349989 ) ) ;
#65745=CARTESIAN_POINT ( 'NONE',  ( 15.50980990363467882, 14.95361599516425244, -1.500000000000002220 ) ) ;
#65747=CARTESIAN_POINT ( 'NONE',  ( -119.6228709571500559, -23.47596703998600631, 11.44779298504227860 ) ) ;
#65749=CARTESIAN_POINT ( 'NONE',  ( -74.62287095715005592, -29.50250243563736774, 8.947779886222143375 ) ) ;
#65750=CARTESIAN_POINT ( 'NONE',  ( 13.56796309060646166, -18.52494293750034871, -1.500000000000002220 ) ) ;
#65753=EDGE_CURVE ( 'NONE', #82055, #72410, #58530, .T. ) ;
#65755=LINE ( 'NONE', #41398, #17538 ) ;
#65756=CARTESIAN_POINT ( 'NONE',  ( -49.60652983502191660, -23.73766607897670156, -1.055555164236457344 ) ) ;
#65757=CARTESIAN_POINT ( 'NONE',  ( 5.780499401231428358, -19.25771307485560158, 11.49999999999999645 ) ) ;
#65760=AXIS2_PLACEMENT_3D ( 'NONE', #34998, #18762, #41625 ) ;
#65761=DIRECTION ( 'NONE',  ( 0.000000000000000000, 0.9999999999976377785, 2.173523156925979128E-06 ) ) ;
#65762=CARTESIAN_POINT ( 'NONE',  ( -65.62287095715005592, -24.99132157543084176, 2.256160258750667502 ) ) ;
#65764=CARTESIAN_POINT ( 'NONE',  ( -18.24115112668064853, 7.888873183027880209, -1.500000000000002220 ) ) ;
#65765=ADVANCED_FACE ( 'NONE', ( #50915 ), #76637, .T. ) ;
#65767=CARTESIAN_POINT ( 'NONE',  ( -113.6312417240655890, -23.48783264082477018, -1.443836473390084363 ) ) ;
#65768=CARTESIAN_POINT ( 'NONE',  ( 10.64064036176630879, -16.58286410872727146, -1.500000000000002220 ) ) ;
#65769=VECTOR ( 'NONE', #10749, 1000.000000000000114 ) ;
#65770=CARTESIAN_POINT ( 'NONE',  ( -60.55620429048339304, -23.48783264082478084, -1.443836473390068820 ) ) ;
#65771=EDGE_CURVE ( 'NONE', #37337, #14386, #32202, .T. ) ;
#65772=EDGE_CURVE ( 'NONE', #89711, #84354, #92770, .T. ) ;
#65776=CARTESIAN_POINT ( 'NONE',  ( -18.82610421443283499, -8.410905081555696938, 11.49999999999999645 ) ) ;
#65777=CARTESIAN_POINT ( 'NONE',  ( -42.62287095715007013, -24.34917612406838217, 0.1852690917426573769 ) ) ;
#65779=CARTESIAN_POINT ( 'NONE',  ( 0.4201012023153268271, 22.63755686032812164, 11.49999999999999645 ) ) ;
#65780=ORIENTED_EDGE ( 'NONE', *, *, #64836, .F. ) ;
#65781=CARTESIAN_POINT ( 'NONE',  ( -126.6228709571500559, -23.47593901973091235, -1.443836447538995760 ) ) ;
#65782=CARTESIAN_POINT ( 'NONE',  ( -97.54990185180675155, -24.34968618360934300, 0.1864209137778855829 ) ) ;
#65783=CARTESIAN_POINT ( 'NONE',  ( -110.6228709571500701, -24.62285846362216191, 9.038163152653526211 ) ) ;
#65785=VERTEX_POINT ( 'NONE', #86727 ) ;
#65786=EDGE_LOOP ( 'NONE', ( #10427, #24596, #10497, #18784 ) ) ;
#65788=CARTESIAN_POINT ( 'NONE',  ( -99.29763458690094069, -25.24802974043947046, 6.184591646183218216 ) ) ;
#65789=CARTESIAN_POINT ( 'NONE',  ( -6.237877366497927234, -22.00199818733190327, 11.49999999999998934 ) ) ;
#65790=CARTESIAN_POINT ( 'NONE',  ( -105.5562042904834072, -24.99132157543166954, 2.256160258750668834 ) ) ;
#65791=CARTESIAN_POINT ( 'NONE',  ( 2.580163054138214562, 21.43444414123800712, -1.500000000000002220 ) ) ;
#65793=LINE ( 'NONE', #12474, #20916 ) ;
#65794=CARTESIAN_POINT ( 'NONE',  ( 15.74396088501716839, 16.14010210793005839, 11.49999999999999645 ) ) ;
#65796=CARTESIAN_POINT ( 'NONE',  ( -33.52287095715006160, -23.48786465467240347, 11.44779295918255357 ) ) ;
#65797=CARTESIAN_POINT ( 'NONE',  ( -12.87221125579857528, -17.80329210173279364, -1.500000000000002220 ) ) ;
#65798=CARTESIAN_POINT ( 'NONE',  ( -44.51365804008561611, -23.73791477778911130, 11.05961554403171121 ) ) ;
#65799=CARTESIAN_POINT ( 'NONE',  ( -29.10172430483776651, -25.21724726705176778, 6.373704058171686171 ) ) ;
#65800=VERTEX_POINT ( 'NONE', #7211 ) ;
#65801=CARTESIAN_POINT ( 'NONE',  ( -89.62287095714998486, -24.51387760970724372, 9.387446482453427166 ) ) ;
#65805=CARTESIAN_POINT ( 'NONE',  ( -5.951451697817415010, -19.63005813332872762, -1.500000000000002220 ) ) ;
#65810=LINE ( 'NONE', #58184, #64922 ) ;
#65811=CARTESIAN_POINT ( 'NONE',  ( -104.5573922987845492, -23.73791477778912196, 11.05961554403170410 ) ) ;
#65812=CARTESIAN_POINT ( 'NONE',  ( -19.36681041099238598, 6.328833669845586485, -1.500000000000002220 ) ) ;
#65815=CARTESIAN_POINT ( 'NONE',  ( -29.48777410446400182, -24.26373688684574503, 9.817618405055078767 ) ) ;
#65816=CARTESIAN_POINT ( 'NONE',  ( -105.5519832311244812, -24.40034930558991633, 0.3402023900116059041 ) ) ;
#65820=CARTESIAN_POINT ( 'NONE',  ( -97.62287095715005592, -24.66019654487200086, 8.947790411086124607 ) ) ;
#65821=ORIENTED_EDGE ( 'NONE', *, *, #79561, .T. ) ;
#65822=CARTESIAN_POINT ( 'NONE',  ( -16.75865769207039335, -12.26659692683164593, 11.49999999999998934 ) ) ;
#65824=CARTESIAN_POINT ( 'NONE',  ( -101.5957409211337392, -23.73766607897670511, -1.055555164236452237 ) ) ;
#65825=ORIENTED_EDGE ( 'NONE', *, *, #89295, .T. ) ;
#65829=CARTESIAN_POINT ( 'NONE',  ( -73.52287095715007581, -24.64898659630528854, 1.056161002820824368 ) ) ;
#65830=ORIENTED_EDGE ( 'NONE', *, *, #50224, .F. ) ;
#65831=VERTEX_POINT ( 'NONE', #84841 ) ;
#65834=CARTESIAN_POINT ( 'NONE',  ( -123.5228709571500616, -24.64965694238408034, 8.947790433994191162 ) ) ;
#65836=LINE ( 'NONE', #90639, #71224 ) ;
#65837=CARTESIAN_POINT ( 'NONE',  ( -74.62287095715008434, -24.50216790748205753, 0.6166512839542480640 ) ) ;
#65838=CARTESIAN_POINT ( 'NONE',  ( 18.88560736741940005, 11.47387103136259690, 11.49999999999999645 ) ) ;
#65839=ORIENTED_EDGE ( 'NONE', *, *, #47151, .T. ) ;
#65840=B_SPLINE_CURVE_WITH_KNOTS ( 'NONE', 3,
 ( #22795, #37548, #61896, #77092 ),
 .UNSPECIFIED., .F., .F.,
 ( 4, 4 ),
 ( 0.000000000000000000, 1.000000000000000000 ),
 .UNSPECIFIED. ) ;
#65841=AXIS2_PLACEMENT_3D ( 'NONE', #70586, #32019, #40141 ) ;
#65842=CARTESIAN_POINT ( 'NONE',  ( -47.62287095715004170, -24.51387760970723662, 9.387446482453421837 ) ) ;
#65843=CARTESIAN_POINT ( 'NONE',  ( -3.801653518169780366, -22.29579330195574016, 11.49999999999998934 ) ) ;
#65844=EDGE_CURVE ( 'NONE', #34495, #34088, #81813, .T. ) ;
#65845=EDGE_CURVE ( 'NONE', #71576, #81001, #91512, .T. ) ;
#65846=AXIS2_PLACEMENT_3D ( 'NONE', #11966, #19574, #42935 ) ;
#65847=B_SPLINE_CURVE_WITH_KNOTS ( 'NONE', 3,
 ( #75257, #97598, #27098, #89492 ),
 .UNSPECIFIED., .F., .F.,
 ( 4, 4 ),
 ( 0.000000000000000000, 9.999999999998897304E-05 ),
 .UNSPECIFIED. ) ;
#65848=EDGE_CURVE ( 'NONE', #14129, #30802, #44258, .T. ) ;
#65849=CARTESIAN_POINT ( 'NONE',  ( -115.6244851806074507, -24.83644354573579349, 8.397322867130093016 ) ) ;
#65850=ORIENTED_EDGE ( 'NONE', *, *, #97309, .T. ) ;
#65851=ORIENTED_EDGE ( 'NONE', *, *, #57176, .T. ) ;
#65854=FACE_OUTER_BOUND ( 'NONE', #3647, .T. ) ;
#65856=CARTESIAN_POINT ( 'NONE',  ( -19.98373207111551508, 7.008865001458166155, 11.49999999999998934 ) ) ;
#65858=PLANE ( 'NONE',  #79 ) ;
#65859=CARTESIAN_POINT ( 'NONE',  ( 19.02167141253037030, -11.55642654327076535, -1.500000000000002220 ) ) ;
#65860=DIRECTION ( 'NONE',  ( -1.000000000000000000, -3.773278334444167608E-23, -8.201307833595939069E-29 ) ) ;
#65863=CARTESIAN_POINT ( 'NONE',  ( -65.62287095715005592, -23.47593901973091235, -1.443836447539006196 ) ) ;
#65865=VECTOR ( 'NONE', #23278, 1000.000000000000114 ) ;
#65866=CARTESIAN_POINT ( 'NONE',  ( -36.48443619261569637, -24.51419770103156637, 9.386484678747175181 ) ) ;
#65868=ADVANCED_FACE ( 'NONE', ( #87737 ), #18222, .F. ) ;
#65869=CARTESIAN_POINT ( 'NONE',  ( -17.32436372870746055, -8.985247798433253053, -1.500000000000002220 ) ) ;
#65870=CARTESIAN_POINT ( 'NONE',  ( -7.526967427842778946, 20.06989004931119425, 11.49999999999998934 ) ) ;
#65871=CARTESIAN_POINT ( 'NONE',  ( -26.85447117215736412, -24.57999539825883772, 1.825772105227124520 ) ) ;
#65872=PLANE ( 'NONE',  #29275 ) ;
#65873=CARTESIAN_POINT ( 'NONE',  ( -77.51234862871442033, -23.96119346886880663, -0.6495511937832126881 ) ) ;
#65874=CARTESIAN_POINT ( 'NONE',  ( 22.20067557195093855, 5.203973054738295190, -1.500000000000002220 ) ) ;
#65877=CARTESIAN_POINT ( 'NONE',  ( -98.58671180656558874, -24.51314013834316086, 0.6176544820404117342 ) ) ;
#65879=CARTESIAN_POINT ( 'NONE',  ( 17.57725459251073019, -9.329341740261039462, 11.49999999999999645 ) ) ;
#65880=CARTESIAN_POINT ( 'NONE',  ( -104.5976451972810679, -23.48783264082477373, -1.443836473390085917 ) ) ;
#65882=CARTESIAN_POINT ( 'NONE',  ( -98.52287095715007581, -23.47593901973090524, -1.443836447538996648 ) ) ;
#65883=ORIENTED_EDGE ( 'NONE', *, *, #98545, .F. ) ;
#65884=CARTESIAN_POINT ( 'NONE',  ( -82.52287095715007581, -24.66019654487199730, 8.947790411086122830 ) ) ;
#65886=EDGE_CURVE ( 'NONE', #52727, #56992, #63688, .T. ) ;
#65887=CARTESIAN_POINT ( 'NONE',  ( -4.559408409702599307, -21.23122434433648209, -1.500000000000002220 ) ) ;
#65888=CARTESIAN_POINT ( 'NONE',  ( -67.58953762381672448, -24.65952944569304606, 1.056160979905700126 ) ) ;
#65889=CARTESIAN_POINT ( 'NONE',  ( -18.58057592369839384, -6.135153870360039896, -1.500000000000002220 ) ) ;
#65891=CARTESIAN_POINT ( 'NONE',  ( -77.62287095715007013, -24.65952944569304606, 1.056160979905699016 ) ) ;
#65894=CARTESIAN_POINT ( 'NONE',  ( -69.62287095715005592, -23.47596703998600631, 11.44779298504227683 ) ) ;
#65895=CARTESIAN_POINT ( 'NONE',  ( -3.558151220431595707, 20.12126150705307381, 11.49999999999999645 ) ) ;
#65897=B_SPLINE_CURVE_WITH_KNOTS ( 'NONE', 3,
 ( #787, #1797, #78397, #2304 ),
 .UNSPECIFIED., .F., .F.,
 ( 4, 4 ),
 ( 0.1205861075877675687, 0.1295925388598832828 ),
 .UNSPECIFIED. ) ;
#65899=CARTESIAN_POINT ( 'NONE',  ( -0.1490770655183801252, -21.12008023607309681, -1.443836447538997758 ) ) ;
#65900=ORIENTED_EDGE ( 'NONE', *, *, #87507, .T. ) ;
#65901=DIRECTION ( 'NONE',  ( -1.000000000000000000, -3.773278334444166432E-23, -8.201307841325785021E-29 ) ) ;
#65904=CARTESIAN_POINT ( 'NONE',  ( -116.5884057677307055, -24.51419770103160189, 9.386484678747169852 ) ) ;
#65906=CARTESIAN_POINT ( 'NONE',  ( -109.5890824698541195, -24.34968618360934300, 0.1864209137778879144 ) ) ;
#65907=EDGE_LOOP ( 'NONE', ( #78193, #18852, #18685, #12892 ) ) ;
#65910=CARTESIAN_POINT ( 'NONE',  ( 16.94363762160741516, 15.55198921429254533, 11.49999999999999645 ) ) ;
#65911=CARTESIAN_POINT ( 'NONE',  ( -4.374245501123523283, 22.36648047097513725, 11.49999999999998934 ) ) ;
#65914=CARTESIAN_POINT ( 'NONE',  ( -49.89338008494267740, -25.20873888344022973, 3.392385934324123387 ) ) ;
#65915=CARTESIAN_POINT ( 'NONE',  ( -54.52287095715005449, -23.48783264082476308, -1.443836473390096797 ) ) ;
#65917=CARTESIAN_POINT ( 'NONE',  ( -21.47987282208850601, -4.139150239982721580, 11.49999999999998934 ) ) ;
#65918=CARTESIAN_POINT ( 'NONE',  ( -69.63096295692471926, -24.35071581493542681, 9.817618358456032368 ) ) ;
#65920=CARTESIAN_POINT ( 'NONE',  ( -90.52287095715006160, -25.00158670708909625, 2.256160236439166411 ) ) ;
#65923=CARTESIAN_POINT ( 'NONE',  ( -8.052747710315523832, 18.77774781879659116, 11.49999999999998934 ) ) ;
#65924=ORIENTED_EDGE ( 'NONE', *, *, #47746, .T. ) ;
#65925=ORIENTED_EDGE ( 'NONE', *, *, #9192, .F. ) ;
#65926=VERTEX_POINT ( 'NONE', #96343 ) ;
#65927=ORIENTED_EDGE ( 'NONE', *, *, #63910, .T. ) ;
#65928=CARTESIAN_POINT ( 'NONE',  ( -22.84742429131147645, -2.885717679200183738, 11.49999999999998934 ) ) ;
#65929=DIRECTION ( 'NONE',  ( 3.773278334444167608E-23, -1.000000000000000000, 0.000000000000000000 ) ) ;
#65930=CARTESIAN_POINT ( 'NONE',  ( 18.63370447891095694, 7.782165041754079304, -1.500000000000002220 ) ) ;
#65931=EDGE_LOOP ( 'NONE', ( #83018, #51455, #24602, #84876 ) ) ;
#65933=CARTESIAN_POINT ( 'NONE',  ( -67.62287095715004170, -24.66019654487199020, 8.947790411086131712 ) ) ;
#65935=CARTESIAN_POINT ( 'NONE',  ( -95.50254368814682948, -24.92564183028979485, 1.928384488918254425 ) ) ;
#65936=CARTESIAN_POINT ( 'NONE',  ( -53.49617477238062691, -24.35071581493542681, 9.817618358456032368 ) ) ;
#65937=CARTESIAN_POINT ( 'NONE',  ( 14.52366289275476419, -15.72616519631134580, 11.49999999999999645 ) ) ;
#65942=CARTESIAN_POINT ( 'NONE',  ( -17.34812393562427246, -13.96779696820907191, -1.500000000000002220 ) ) ;
#65943=CARTESIAN_POINT ( 'NONE',  ( -20.26430336558559020, 4.098603726722801710, 11.49999999999998934 ) ) ;
#65944=ORIENTED_EDGE ( 'NONE', *, *, #49118, .T. ) ;
#65948=CARTESIAN_POINT ( 'NONE',  ( -129.5228709571500758, -23.47593901973090524, -1.443836447538996204 ) ) ;
#65949=VERTEX_POINT ( 'NONE', #65920 ) ;
#65952=CARTESIAN_POINT ( 'NONE',  ( -16.25153318171239647, -13.25006309444557751, -1.500000000000002220 ) ) ;
#65953=CARTESIAN_POINT ( 'NONE',  ( 13.84421170697429737, -16.98027460053469895, 11.49999999999999645 ) ) ;
#65955=CARTESIAN_POINT ( 'NONE',  ( -73.50294862231642412, -24.35071581493543036, 9.817618358456027039 ) ) ;
#65956=CARTESIAN_POINT ( 'NONE',  ( -22.50818191331092777, 0.9639279967183422837, -1.500000000000002220 ) ) ;
#65959=CARTESIAN_POINT ( 'NONE',  ( 0.7041596644206948863, -20.94928778062849162, -1.500000000000002220 ) ) ;
#65960=CARTESIAN_POINT ( 'NONE',  ( -26.10989220437014424, -24.88148810348265627, 5.384403059502965050 ) ) ;
#65962=CARTESIAN_POINT ( 'NONE',  ( -72.62287095715001328, -24.33832256526968507, 0.1851278514119847063 ) ) ;
#65963=CARTESIAN_POINT ( 'NONE',  ( -91.62287095715004170, -24.64965695001468404, 8.947790433994180503 ) ) ;
#65965=VERTEX_POINT ( 'NONE', #50177 ) ;
#65966=ORIENTED_EDGE ( 'NONE', *, *, #58166, .F. ) ;
#65967=CARTESIAN_POINT ( 'NONE',  ( -44.52287095715004739, -24.51387760970726148, 9.387446482453421837 ) ) ;
#65969=VECTOR ( 'NONE', #32318, 1000.000000000000114 ) ;
#65970=B_SPLINE_CURVE_WITH_KNOTS ( 'NONE', 3,
 ( #84249, #53820, #14734, #76626 ),
 .UNSPECIFIED., .F., .F.,
 ( 4, 4 ),
 ( 0.000000000000000000, 9.999999999996123101E-05 ),
 .UNSPECIFIED. ) ;
#65971=CARTESIAN_POINT ( 'NONE',  ( 20.52986552169224410, -6.224258026782483633, -1.500000000000002220 ) ) ;
#65975=CARTESIAN_POINT ( 'NONE',  ( -16.00611555608923098, 13.71732778110762219, -1.500000000000002220 ) ) ;
#65978=DIRECTION ( 'NONE',  ( 1.000000000000000000, 3.773278334444167608E-23, 8.201307833595939069E-29 ) ) ;
#65980=CARTESIAN_POINT ( 'NONE',  ( -101.5487956542387451, -24.51314013834316086, 0.6176544820404185065 ) ) ;
#65981=CARTESIAN_POINT ( 'NONE',  ( -129.5898459561496168, -23.96169478059714564, 10.65365249895717348 ) ) ;
#65982=CARTESIAN_POINT ( 'NONE',  ( -2.366842300981895519, -21.98859952056468714, -1.500000000000002220 ) ) ;
#65983=EDGE_LOOP ( 'NONE', ( #71506, #49729, #30591, #16097 ) ) ;
#65984=B_SPLINE_CURVE_WITH_KNOTS ( 'NONE', 3,
 ( #35554, #66524, #50278, #90825 ),
 .UNSPECIFIED., .F., .F.,
 ( 4, 4 ),
 ( 0.2306647120247341254, 0.2396711432968496869 ),
 .UNSPECIFIED. ) ;
#65985=CARTESIAN_POINT ( 'NONE',  ( -81.58821135512123135, -24.35071581493543391, 9.817618358456037697 ) ) ;
#65986=DIRECTION ( 'NONE',  ( 0.000000000000000000, -0.9999999999976377785, -2.173523156925979975E-06 ) ) ;
#65987=CARTESIAN_POINT ( 'NONE',  ( -41.77207742203299290, -25.31624564944289091, 4.730364161577088389 ) ) ;
#65988=CARTESIAN_POINT ( 'NONE',  ( -26.97027047204615968, -24.54739053293899786, 1.590605884330588360 ) ) ;
#65991=CARTESIAN_POINT ( 'NONE',  ( 19.36035776617087123, -9.008237321879198234, 11.49999999999998934 ) ) ;
#65992=DIRECTION ( 'NONE',  ( -3.773278334453079618E-23, 0.9999999999976377785, 2.173523156925979975E-06 ) ) ;
#65993=CARTESIAN_POINT ( 'NONE',  ( -51.95422829247385721, -25.11539320716599377, 2.804431449967496714 ) ) ;
#65994=CARTESIAN_POINT ( 'NONE',  ( -64.49990038984530827, -24.35071581493543391, 9.817618358456023486 ) ) ;
#65996=CARTESIAN_POINT ( 'NONE',  ( -0.2110286175373513040, -22.56517410205234597, -1.500000000000002220 ) ) ;
#65998=ORIENTED_EDGE ( 'NONE', *, *, #75188, .F. ) ;
#66000=CARTESIAN_POINT ( 'NONE',  ( -70.22287095715009286, -23.47593901973090524, -1.443836447538997980 ) ) ;
#66001=CARTESIAN_POINT ( 'NONE',  ( -10.60818629614422370, 16.63341085705455669, 11.49999999999999645 ) ) ;
#66004=CARTESIAN_POINT ( 'NONE',  ( -119.5228709571501753, -23.73907113216990439, -1.053371485793245688 ) ) ;
#66005=ORIENTED_EDGE ( 'NONE', *, *, #41936, .F. ) ;
#66007=CARTESIAN_POINT ( 'NONE',  ( -29.40205842853959339, -24.60094121823534508, 2.693430781335976576 ) ) ;
#66008=DIRECTION ( 'NONE',  ( -3.773278334453079030E-23, 0.9999999999976377785, 2.173523156925979128E-06 ) ) ;
#66009=CARTESIAN_POINT ( 'NONE',  ( -14.23256820581467785, 16.29125061305494526, -1.500000000000002220 ) ) ;
#66011=CARTESIAN_POINT ( 'NONE',  ( -76.58953762381673869, -24.64898659630367916, 1.056161002820385830 ) ) ;
#66014=CARTESIAN_POINT ( 'NONE',  ( -118.6228709571500559, -24.64965695001469115, 8.947790433994175174 ) ) ;
#66016=CARTESIAN_POINT ( 'NONE',  ( 16.35176858736616978, 11.14859404531058473, -1.500000000000002220 ) ) ;
#66017=VERTEX_POINT ( 'NONE', #58294 ) ;
#66019=CARTESIAN_POINT ( 'NONE',  ( -5.286950244708777724, -19.55949958832428948, 11.49999999999999645 ) ) ;
#66021=ADVANCED_FACE ( 'NONE', ( #89232 ), #74009, .F. ) ;
#66024=ORIENTED_EDGE ( 'NONE', *, *, #59567, .F. ) ;
#66026=CARTESIAN_POINT ( 'NONE',  ( -102.5562042904833788, -23.48783264082478084, -1.443836473390062825 ) ) ;
#66029=CARTESIAN_POINT ( 'NONE',  ( -33.62287095715005592, -23.48783264082477373, -1.443836473390074371 ) ) ;
#66030=CARTESIAN_POINT ( 'NONE',  ( 15.84714387567644955, -12.28532832577633194, -1.500000000000002220 ) ) ;
#66031=DIRECTION ( 'NONE',  ( -3.773278334453079618E-23, 0.9999999999976377785, 2.173523156925979975E-06 ) ) ;
#66032=VERTEX_POINT ( 'NONE', #11104 ) ;
#66033=VECTOR ( 'NONE', #1059, 1000.000000000000114 ) ;
#66034=CARTESIAN_POINT ( 'NONE',  ( -50.27385278553439463, -25.31297216834682473, 4.732894841895117999 ) ) ;
#66036=CARTESIAN_POINT ( 'NONE',  ( -92.62287095715009855, -24.33927499327855415, 9.819080762295817166 ) ) ;
#66043=AXIS2_PLACEMENT_3D ( 'NONE', #47223, #21861, #14754 ) ;
#66044=CARTESIAN_POINT ( 'NONE',  ( 19.83649001621966335, 4.521578618930774951, -1.500000000000002220 ) ) ;
#66046=CARTESIAN_POINT ( 'NONE',  ( -16.74478417649319084, -15.65585335247391896, 11.49999999999998934 ) ) ;
#66048=EDGE_LOOP ( 'NONE', ( #9017, #54680, #91077, #86668 ) ) ;
#66049=CARTESIAN_POINT ( 'NONE',  ( -37.62287095715008434, -23.94994826722515313, -0.6494450866351710872 ) ) ;
#66050=CARTESIAN_POINT ( 'NONE',  ( -49.51155500790866171, -25.26264100752995745, 6.743855136296660113 ) ) ;
#66052=CARTESIAN_POINT ( 'NONE',  ( -14.79452276021403634, 15.15755283273500531, 11.49999999999999645 ) ) ;
#66053=CARTESIAN_POINT ( 'NONE',  ( -15.97456084408017674, 15.39233244482803009, -1.500000000000002220 ) ) ;
#66054=CARTESIAN_POINT ( 'NONE',  ( -6.273408026305254737, 19.60348359158234288, 11.49999999999998934 ) ) ;
#66055=ORIENTED_EDGE ( 'NONE', *, *, #36199, .T. ) ;
#66056=CARTESIAN_POINT ( 'NONE',  ( -41.60044768456533859, -23.96119346886880663, -0.6495511937831990323 ) ) ;
#66057=ORIENTED_EDGE ( 'NONE', *, *, #91909, .T. ) ;
#66059=DIRECTION ( 'NONE',  ( 3.773278334444166432E-23, -1.000000000000000000, 0.000000000000000000 ) ) ;
#66061=EDGE_CURVE ( 'NONE', #30450, #1347, #62409, .T. ) ;
#66062=ORIENTED_EDGE ( 'NONE', *, *, #82207, .F. ) ;
#66064=ORIENTED_EDGE ( 'NONE', *, *, #20421, .T. ) ;
#66065=CARTESIAN_POINT ( 'NONE',  ( -111.7334199135079302, -25.26981769024641267, 3.943713881720887660 ) ) ;
#66066=CARTESIAN_POINT ( 'NONE',  ( -28.47397640525979412, -24.49582855094319811, 8.947790409070464079 ) ) ;
#66068=CARTESIAN_POINT ( 'NONE',  ( -20.73834036848188234, 1.213307192923735345, -1.500000000000002220 ) ) ;
#66069=CARTESIAN_POINT ( 'NONE',  ( 21.38347125639554136, -3.707035686939989638, 11.49999999999999645 ) ) ;
#66071=EDGE_CURVE ( 'NONE', #61182, #50986, #91711, .T. ) ;
#66072=CARTESIAN_POINT ( 'NONE',  ( -52.52287095715006870, -24.64898659630367916, 1.056161002820821038 ) ) ;
#66073=CARTESIAN_POINT ( 'NONE',  ( -115.6284389687382230, -24.15503026093916716, -0.2815557561904330486 ) ) ;
#66074=CARTESIAN_POINT ( 'NONE',  ( -5.254942042970298210, 21.81482460008805546, -1.500000000000002220 ) ) ;
#66075=EDGE_CURVE ( 'NONE', #83889, #8604, #28829, .T. ) ;
#66078=EDGE_LOOP ( 'NONE', ( #38311, #61430, #82869, #66685 ) ) ;
#66080=DIRECTION ( 'NONE',  ( 0.000000000000000000, -0.9999999999976377785, -2.173523156925979128E-06 ) ) ;
#66081=B_SPLINE_SURFACE_WITH_KNOTS ( 'NONE', 3, 3, ( 
 ( #17891, #79779, #27003, #87906 ),
 ( #49862, #33616, #34623, #10276 ),
 ( #55966, #41233, #95009, #86893 ),
 ( #63586, #1671, #72188, #64597 ),
 ( #40229, #96014, #94508, #72685 ),
 ( #11274, #9772, #56471, #95512 ),
 ( #48348, #32610, #73186, #25998 ) ),
 .UNSPECIFIED., .F., .F., .F.,
 ( 4, 3, 4 ),
 ( 4, 4 ),
 ( 0.7945040050992243641, 0.8970133687736501216, 0.9995227324480757680 ),
 ( 0.2695624968113854436, 0.2706996693028251300 ),
 .UNSPECIFIED. ) ;
#66082=EDGE_CURVE ( 'NONE', #80731, #58107, #58816, .T. ) ;
#66085=EDGE_CURVE ( 'NONE', #3648, #82610, #90728, .T. ) ;
#66088=ORIENTED_EDGE ( 'NONE', *, *, #69713, .T. ) ;
#66089=CARTESIAN_POINT ( 'NONE',  ( 19.98943718749924159, -7.363913660680385220, -1.500000000000002220 ) ) ;
#66091=CARTESIAN_POINT ( 'NONE',  ( -88.50537230221658547, -24.51314013834315375, 0.6176544820404129554 ) ) ;
#66092=CARTESIAN_POINT ( 'NONE',  ( -0.06377455873143267340, 21.83884041771831619, -1.500000000000002220 ) ) ;
#66093=FACE_OUTER_BOUND ( 'NONE', #89888, .T. ) ;
#66094=CARTESIAN_POINT ( 'NONE',  ( -20.89466310375201985, -8.809181082428260368, 11.49999999999998934 ) ) ;
#66095=CARTESIAN_POINT ( 'NONE',  ( -39.62287095715005592, -29.50247984919015209, -1.443849546365060466 ) ) ;
#66096=PLANE ( 'NONE',  #20629 ) ;
#66097=CARTESIAN_POINT ( 'NONE',  ( 16.32745387341675780, -14.53119815553504068, -1.500000000000002220 ) ) ;
#66098=CARTESIAN_POINT ( 'NONE',  ( -66.62287095715009855, -24.34917612406837861, 0.1852690917426618733 ) ) ;
#66099=ORIENTED_EDGE ( 'NONE', *, *, #3070, .F. ) ;
#66101=CARTESIAN_POINT ( 'NONE',  ( -69.62287095715005592, -24.65952944569304961, 1.056160979905697017 ) ) ;
#66102=CARTESIAN_POINT ( 'NONE',  ( -49.06509223983938739, -25.26337459480267000, 6.860564339532760236 ) ) ;
#66105=CARTESIAN_POINT ( 'NONE',  ( -90.62287095715004170, -23.48783264082478794, -1.443836473390063713 ) ) ;
#66106=ORIENTED_EDGE ( 'NONE', *, *, #28304, .F. ) ;
#66109=CARTESIAN_POINT ( 'NONE',  ( -4.916304867406160461, -20.68799595667769964, -1.500000000000002220 ) ) ;
#66110=FACE_OUTER_BOUND ( 'NONE', #70686, .T. ) ;
#66111=CARTESIAN_POINT ( 'NONE',  ( -27.27594984642231069, -24.97064415668394233, 2.337720463694722195 ) ) ;
#66112=CARTESIAN_POINT ( 'NONE',  ( -85.50395841013464349, -24.52300882791530157, 0.6510814631126307095 ) ) ;
#66114=CARTESIAN_POINT ( 'NONE',  ( -68.56535840407821070, -23.48783264082477018, -1.443836473390095243 ) ) ;
#66115=CARTESIAN_POINT ( 'NONE',  ( -44.62287095715004170, -24.33927499327853639, 9.819080762295815390 ) ) ;
#66116=ORIENTED_EDGE ( 'NONE', *, *, #5093, .F. ) ;
#66117=CARTESIAN_POINT ( 'NONE',  ( -0.4769873229303308038, -19.55164744950295841, 11.49999999999999645 ) ) ;
#66118=CARTESIAN_POINT ( 'NONE',  ( -66.62287095715005592, -23.48786465467241058, 11.44779295918254647 ) ) ;
#66120=CARTESIAN_POINT ( 'NONE',  ( -29.03447252004092505, -24.88235332209834993, 7.704480964116209307 ) ) ;
#66121=ADVANCED_FACE ( 'NONE', ( #84107 ), #14590, .F. ) ;
#66122=ORIENTED_EDGE ( 'NONE', *, *, #37976, .T. ) ;
#66123=CARTESIAN_POINT ( 'NONE',  ( -117.5228709571501469, -24.33927499327855770, 9.819080762295802955 ) ) ;
#66124=CARTESIAN_POINT ( 'NONE',  ( -101.9507253916653440, -25.24282061761981666, 6.236250683194342059 ) ) ;
#66126=CARTESIAN_POINT ( 'NONE',  ( -81.43785252974821276, -25.03155984298766867, 7.210847909229809005 ) ) ;
#66127=CARTESIAN_POINT ( 'NONE',  ( 3.778003860535555702, 19.31821889988591323, 11.49999999999998934 ) ) ;
#66129=CARTESIAN_POINT ( 'NONE',  ( 5.514125806255895004E-17, -29.50250243563665720, 8.947779561265919668 ) ) ;
#66132=EDGE_CURVE ( 'NONE', #8769, #96261, #60094, .T. ) ;
#66134=CARTESIAN_POINT ( 'NONE',  ( -54.52287095715010423, -23.95044443724992789, 10.65354141964649237 ) ) ;
#66136=LINE ( 'NONE', #35664, #19907 ) ;
#66138=PLANE ( 'NONE',  #54806 ) ;
#66139=CARTESIAN_POINT ( 'NONE',  ( -102.5228709571500758, -29.50250243563736774, 8.947779886222138046 ) ) ;
#66141=CARTESIAN_POINT ( 'NONE',  ( 15.91301918423788919, -12.03417825965012433, -1.500000000000002220 ) ) ;
#66142=EDGE_CURVE ( 'NONE', #76257, #71901, #80555, .T. ) ;
#66143=CARTESIAN_POINT ( 'NONE',  ( -0.1307260668091378419, -21.35764833532042672, 11.26293215892713206 ) ) ;
#66144=CARTESIAN_POINT ( 'NONE',  ( -4.359361796094493258, -19.42695174060331809, -1.500000000000002220 ) ) ;
#66146=VECTOR ( 'NONE', #28258, 1000.000000000000114 ) ;
#66148=B_SPLINE_CURVE_WITH_KNOTS ( 'NONE', 3,
 ( #26247, #34859, #40975, #42981, #10016, #57220, #50094, #27744, #96260, #88652, #81034, #42492 ),
 .UNSPECIFIED., .F., .F.,
 ( 4, 2, 2, 2, 2, 4 ),
 ( 8.673617379884034509E-19, 0.0002001096462788820726, 0.0004002192925577632778, 0.0008004385851155264471, 0.001200657877673289454, 0.001600877170231052677 ),
 .UNSPECIFIED. ) ;
#66149=( NAMED_UNIT ( * ) PLANE_ANGLE_UNIT ( ) SI_UNIT ( $, .RADIAN. ) );
#66152=CARTESIAN_POINT ( 'NONE',  ( -105.6228709571500559, -29.50247984919015209, -1.443849546365048253 ) ) ;
#66157=B_SPLINE_SURFACE_WITH_KNOTS ( 'NONE', 3, 3, ( 
 ( #70157, #47327, #39198, #55443 ),
 ( #32088, #78250, #70661, #17370 ),
 ( #62054, #25481, #77248, #1151 ),
 ( #1655, #63570, #640, #63063 ),
 ( #92980, #62554, #93986, #94491 ),
 ( #94991, #87380, #48333, #23454 ),
 ( #31589, #24974, #56455, #24476 ) ),
 .UNSPECIFIED., .F., .F., .F.,
 ( 4, 3, 4 ),
 ( 4, 4 ),
 ( 0.7945040050992243641, 0.8970133687736505657, 0.9995227324480766562 ),
 ( 0.8297048367401780311, 0.8311006081063124773 ),
 .UNSPECIFIED. ) ;
#66158=CARTESIAN_POINT ( 'NONE',  ( -62.62287095715003460, -23.72747288104441665, -1.053458166803662888 ) ) ;
#66159=CARTESIAN_POINT ( 'NONE',  ( -65.52287095715006160, -29.50247984919015209, -1.443849546365055359 ) ) ;
#66161=CARTESIAN_POINT ( 'NONE',  ( -6.993686169601437186, 18.98418669460116348, 11.49999999999998934 ) ) ;
#66162=B_SPLINE_CURVE_WITH_KNOTS ( 'NONE', 3,
 ( #86837, #64544, #87851, #41179 ),
 .UNSPECIFIED., .F., .F.,
 ( 4, 4 ),
 ( 0.1488646418289148732, 0.1498653888696803438 ),
 .UNSPECIFIED. ) ;
#66166=DIRECTION ( 'NONE',  ( -3.773278334453079030E-23, 0.9999999999976377785, 2.173523156925979128E-06 ) ) ;
#66168=CARTESIAN_POINT ( 'NONE',  ( -79.37676797629123371, -25.29665582273151614, 5.684420612865764610 ) ) ;
#66170=CARTESIAN_POINT ( 'NONE',  ( -13.75281105048956576, 14.62798779934380811, -1.500000000000002220 ) ) ;
#66171=CARTESIAN_POINT ( 'NONE',  ( 20.15827220212406701, 6.050813824765241655, 11.49999999999999645 ) ) ;
#66172=CARTESIAN_POINT ( 'NONE',  ( -48.87380231474225667, -29.50249632652208476, 6.137082770844160429 ) ) ;
#66173=CARTESIAN_POINT ( 'NONE',  ( -70.59772795895749198, -24.15602025860896518, 10.28564288303534724 ) ) ;
#66174=CARTESIAN_POINT ( 'NONE',  ( -14.46940225681120396, -16.66540133702554272, 11.49999999999998934 ) ) ;
#66176=CARTESIAN_POINT ( 'NONE',  ( -39.51244657141699435, -25.27805987054186687, 4.531907366321720865 ) ) ;
#66178=CARTESIAN_POINT ( 'NONE',  ( -64.58953762381673869, -23.47596703998600276, 11.44779298504227505 ) ) ;
#66180=CARTESIAN_POINT ( 'NONE',  ( -72.49894236110185375, -24.51314013834316796, 0.6176544820404143987 ) ) ;
#66182=EDGE_LOOP ( 'NONE', ( #44108, #77728, #16594, #43161 ) ) ;
#66184=ORIENTED_EDGE ( 'NONE', *, *, #76159, .T. ) ;
#66185=FACE_OUTER_BOUND ( 'NONE', #33121, .T. ) ;
#66186=CARTESIAN_POINT ( 'NONE',  ( -72.58953762381671027, -23.48786465467241058, 11.44779295918254647 ) ) ;
#66187=CARTESIAN_POINT ( 'NONE',  ( -76.60092789896461341, -23.73766607897670866, -1.055555164236452681 ) ) ;
#66188=CARTESIAN_POINT ( 'NONE',  ( 17.30552477474510908, -11.17933342135444086, -1.500000000000002220 ) ) ;
#66189=CARTESIAN_POINT ( 'NONE',  ( -0.8555947871142663974, 21.52075748220454798, 11.49999999999999645 ) ) ;
#66194=CARTESIAN_POINT ( 'NONE',  ( 4.697571063781373013, 21.84268702631108994, -1.500000000000002220 ) ) ;
#66196=CARTESIAN_POINT ( 'NONE',  ( -124.6228709571500701, -24.34917612406838927, 0.1852690917426691730 ) ) ;
#66201=CARTESIAN_POINT ( 'NONE',  ( 20.57277012135545036, 3.371850554975475145, -1.500000000000002220 ) ) ;
#66205=ORIENTED_EDGE ( 'NONE', *, *, #83242, .F. ) ;
#66206=EDGE_LOOP ( 'NONE', ( #87625, #55763, #25129, #82396 ) ) ;
#66207=CARTESIAN_POINT ( 'NONE',  ( -100.5044678508139810, -25.00182538069147142, 7.747789668545045139 ) ) ;
#66208=CARTESIAN_POINT ( 'NONE',  ( 11.07546443054301655, -17.96822238807187233, -1.500000000000002220 ) ) ;
#66210=CARTESIAN_POINT ( 'NONE',  ( -53.62287095715005592, -29.50248528299804818, 1.056150453629033370 ) ) ;
#66211=CARTESIAN_POINT ( 'NONE',  ( -110.6228709571500559, -24.99132157543166954, 2.256160258750667502 ) ) ;
#66212=CARTESIAN_POINT ( 'NONE',  ( -129.5228709571500758, -23.48786465467242479, 11.44779295918253581 ) ) ;
#66213=FACE_OUTER_BOUND ( 'NONE', #43498, .T. ) ;
#66215=CARTESIAN_POINT ( 'NONE',  ( -2.129050106866105185, 21.58297100922832357, -1.500000000000002220 ) ) ;
#66216=CARTESIAN_POINT ( 'NONE',  ( -63.52287095715003318, -23.73934037231756022, 11.05740245334328797 ) ) ;
#66217=CARTESIAN_POINT ( 'NONE',  ( -19.03210976516136554, 11.49075778266564107, 11.49999999999999645 ) ) ;
#66218=ORIENTED_EDGE ( 'NONE', *, *, #99973, .T. ) ;
#66219=EDGE_CURVE ( 'NONE', #41736, #53720, #27366, .T. ) ;
#66220=CARTESIAN_POINT ( 'NONE',  ( -50.61185169649064619, -25.31441726102578116, 5.215440883357011614 ) ) ;
#66224=LINE ( 'NONE', #97145, #19926 ) ;
#66227=CARTESIAN_POINT ( 'NONE',  ( -101.1409834047034906, -25.16687399051181018, 6.899440319863159310 ) ) ;
#66228=CARTESIAN_POINT ( 'NONE',  ( -108.8968792378192063, -25.15277794460069316, 6.986250878905963191 ) ) ;
#66229=CARTESIAN_POINT ( 'NONE',  ( -43.62287095715002749, -24.33927499327853639, 9.819080762295822495 ) ) ;
#66232=ORIENTED_EDGE ( 'NONE', *, *, #46228, .T. ) ;
#66233=CARTESIAN_POINT ( 'NONE',  ( -19.23900614489824079, 2.250179475969715348, 11.49999999999999645 ) ) ;
#66235=CARTESIAN_POINT ( 'NONE',  ( 22.31695869535024102, -2.478243017838637652, -1.500000000000002220 ) ) ;
#66236=ORIENTED_EDGE ( 'NONE', *, *, #55333, .F. ) ;
#66237=CARTESIAN_POINT ( 'NONE',  ( -101.6292210487389269, -24.15620529776628800, 10.23563542870660292 ) ) ;
#66238=LINE ( 'NONE', #5306, #47448 ) ;
#66239=CARTESIAN_POINT ( 'NONE',  ( -116.5228709571500474, -23.94994826722564696, -0.6494450866342714734 ) ) ;
#66241=CARTESIAN_POINT ( 'NONE',  ( -63.92537901004148893, -24.57143472585066490, 0.8294870405985537154 ) ) ;
#66243=CARTESIAN_POINT ( 'NONE',  ( 16.73968668634701729, 10.17700309559984717, 11.49999999999998934 ) ) ;
#66244=CARTESIAN_POINT ( 'NONE',  ( -46.54049122901287916, -24.34968618360933235, 0.1864209137778778391 ) ) ;
#66245=ORIENTED_EDGE ( 'NONE', *, *, #61716, .F. ) ;
#66246=CARTESIAN_POINT ( 'NONE',  ( -21.46803524902295024, 1.580295693706654347, -1.500000000000002220 ) ) ;
#66247=CARTESIAN_POINT ( 'NONE',  ( -129.5228709571500758, -24.64965694238408034, 8.947790433994189385 ) ) ;
#66248=CARTESIAN_POINT ( 'NONE',  ( -80.64958649024407578, -25.31572648974913164, 4.980655863047315890 ) ) ;
#66249=DIRECTION ( 'NONE',  ( -1.000000000000000000, -3.773278334444166432E-23, -8.201307841325785021E-29 ) ) ;
#66250=DIRECTION ( 'NONE',  ( -3.773278334453079030E-23, 0.9999999999976377785, 2.173523156925979128E-06 ) ) ;
#66251=CARTESIAN_POINT ( 'NONE',  ( 8.272623322502495213, 21.45567517505680044, -1.500000000000002220 ) ) ;
#66253=B_SPLINE_CURVE_WITH_KNOTS ( 'NONE', 3,
 ( #2870, #81481, #95699, #79471, #27694, #88098 ),
 .UNSPECIFIED., .F., .F.,
 ( 4, 2, 4 ),
 ( 6.391158118975501388E-06, 0.001387004593080795036, 0.002767618028042614572 ),
 .UNSPECIFIED. ) ;
#66255=LINE ( 'NONE', #93538, #98498 ) ;
#66256=CARTESIAN_POINT ( 'NONE',  ( -49.62828767225136062, -24.51314013834316086, 0.6176544820404115121 ) ) ;
#66257=CARTESIAN_POINT ( 'NONE',  ( -14.05898297266747221, -14.31596314050798568, 11.49999999999999645 ) ) ;
#66258=CARTESIAN_POINT ( 'NONE',  ( -108.9545715455115129, -25.10927687032588906, 4.170145204219119606 ) ) ;
#66259=CARTESIAN_POINT ( 'NONE',  ( -31.52287095715004739, -23.48783264083373723, -1.443836473376154617 ) ) ;
#66263=CARTESIAN_POINT ( 'NONE',  ( -95.62287095715005592, -23.47596703998600631, 11.44779298504227860 ) ) ;
#66264=CARTESIAN_POINT ( 'NONE',  ( -13.97081141688431138, 14.13901428111770819, 11.49999999999998934 ) ) ;
#66265=CARTESIAN_POINT ( 'NONE',  ( -109.5228709571500616, -24.64898659630530275, 1.056161002820831474 ) ) ;
#66266=CARTESIAN_POINT ( 'NONE',  ( 17.05426814964238957, 9.943002105365778220, -1.500000000000002220 ) ) ;
#66268=CARTESIAN_POINT ( 'NONE',  ( -110.5228709571501184, -24.91570333825771755, 8.075032458260348989 ) ) ;
#66270=CARTESIAN_POINT ( 'NONE',  ( 20.45670835789597319, 2.398913822417158226, 11.49999999999999645 ) ) ;
#66271=ADVANCED_FACE ( 'NONE', ( #68394 ), #84609, .F. ) ;
#66273=CARTESIAN_POINT ( 'NONE',  ( 16.59953334139655468, -15.42474913338910980, 11.49999999999999645 ) ) ;
#66274=ORIENTED_EDGE ( 'NONE', *, *, #24573, .F. ) ;
#66275=CARTESIAN_POINT ( 'NONE',  ( -62.52287095715006160, -24.64965694238406613, 8.947790433994201820 ) ) ;
#66277=CARTESIAN_POINT ( 'NONE',  ( -110.5228709571500332, -24.92579138211018730, 1.929029949965659352 ) ) ;
#66279=EDGE_CURVE ( 'NONE', #37096, #100315, #30943, .T. ) ;
#66280=ORIENTED_EDGE ( 'NONE', *, *, #26170, .T. ) ;
#66283=CARTESIAN_POINT ( 'NONE',  ( -21.29394331855728240, -8.360804490491451801, 11.49999999999998934 ) ) ;
#66284=CARTESIAN_POINT ( 'NONE',  ( -74.62287095715005592, -24.65952944569304606, 1.056160979905696351 ) ) ;
#66285=CARTESIAN_POINT ( 'NONE',  ( 15.64208908530913256, 14.88810259432246852, -1.500000000000002220 ) ) ;
#66286=PLANE ( 'NONE',  #44719 ) ;
#66287=CARTESIAN_POINT ( 'NONE',  ( -65.52287095715004739, -23.85196035786901092, -0.8779234886475200117 ) ) ;
#66288=CARTESIAN_POINT ( 'NONE',  ( -0.06565682164858396841, -22.51586213336150166, 11.49999999999999645 ) ) ;
#66289=VERTEX_POINT ( 'NONE', #29821 ) ;
#66290=CARTESIAN_POINT ( 'NONE',  ( -86.62287095715004170, -23.47593901973091235, -1.443836447539002865 ) ) ;
#66291=CARTESIAN_POINT ( 'NONE',  ( -18.27885182143903720, 12.20952002138517045, 11.49999999999998934 ) ) ;
#66292=CARTESIAN_POINT ( 'NONE',  ( -111.5222191420114370, -23.48783264082477018, -1.443836473390086805 ) ) ;
#66293=LINE ( 'NONE', #43449, #76196 ) ;
#66294=ORIENTED_EDGE ( 'NONE', *, *, #31083, .T. ) ;
#66295=DIRECTION ( 'NONE',  ( 0.000000000000000000, 0.9999999999976377785, 2.173523156925979975E-06 ) ) ;
#66303=EDGE_CURVE ( 'NONE', #84371, #1776, #69889, .T. ) ;
#66304=ORIENTED_EDGE ( 'NONE', *, *, #81869, .F. ) ;
#66305=EDGE_CURVE ( 'NONE', #36107, #13848, #16384, .T. ) ;
#66307=CARTESIAN_POINT ( 'NONE',  ( -115.5228709571500616, -29.50248528299804818, 1.056150453629045360 ) ) ;
#66309=CARTESIAN_POINT ( 'NONE',  ( -14.48729221511043441, 14.40292172154154926, -1.500000000000002220 ) ) ;
#66310=EDGE_LOOP ( 'NONE', ( #93354, #66950, #47974, #24127 ) ) ;
#66312=AXIS2_PLACEMENT_3D ( 'NONE', #80018, #83503, #43467 ) ;
#66313=CARTESIAN_POINT ( 'NONE',  ( -51.61964320672224460, -25.23391071228556370, 3.593176832712704716 ) ) ;
#66314=CARTESIAN_POINT ( 'NONE',  ( -105.5221828617972619, -23.48783264082477018, -1.443836473390094355 ) ) ;
#66315=CARTESIAN_POINT ( 'NONE',  ( -71.31671495077925726, -25.03149765108591751, 7.173522054403384196 ) ) ;
#66317=CARTESIAN_POINT ( 'NONE',  ( -28.94548163072471425, -24.76881035311403423, 3.108274031987006136 ) ) ;
#66318=CARTESIAN_POINT ( 'NONE',  ( -27.85310238079214784, -25.26248076281864741, 8.249330725495340744 ) ) ;
#66320=AXIS2_PLACEMENT_3D ( 'NONE', #94575, #25057, #72757 ) ;
#66321=CARTESIAN_POINT ( 'NONE',  ( -16.26442346200556344, 12.93145763113255775, 11.49999999999998934 ) ) ;
#66323=ORIENTED_EDGE ( 'NONE', *, *, #81691, .F. ) ;
#66324=CARTESIAN_POINT ( 'NONE',  ( -40.17256793773198353, -25.30544673913221487, 5.061440930064124544 ) ) ;
#66331=CARTESIAN_POINT ( 'NONE',  ( -33.52287095715006160, -24.50321055353803956, 9.387540953477525818 ) ) ;
#66333=CARTESIAN_POINT ( 'NONE',  ( -116.6228709571500417, -24.66019654487199730, 8.947790411086121054 ) ) ;
#66334=CARTESIAN_POINT ( 'NONE',  ( -113.5895376238167245, -23.47593901973091235, -1.443836447538999312 ) ) ;
#66335=CARTESIAN_POINT ( 'NONE',  ( -71.26908920811321480, -25.24515179469667814, 5.945032366209153984 ) ) ;
#66336=CARTESIAN_POINT ( 'NONE',  ( 22.05266032001784637, -1.487345182339283367, 11.49999999999999645 ) ) ;
#66339=CARTESIAN_POINT ( 'NONE',  ( -72.62287095715009855, -24.34917612406838217, 0.1852690917426622341 ) ) ;
#66340=CARTESIAN_POINT ( 'NONE',  ( 21.71239400539012721, -6.292901409244172406, -1.500000000000002220 ) ) ;
#66341=EDGE_CURVE ( 'NONE', #85588, #17471, #39938, .T. ) ;
#66342=CARTESIAN_POINT ( 'NONE',  ( -99.55486036248895232, -25.30557962015589979, 4.972970070441952828 ) ) ;
#66343=ORIENTED_EDGE ( 'NONE', *, *, #74495, .T. ) ;
#66344=B_SPLINE_CURVE_WITH_KNOTS ( 'NONE', 3,
 ( #59679, #20095, #34835, #50065 ),
 .UNSPECIFIED., .F., .F.,
 ( 4, 4 ),
 ( 0.000000000000000000, 9.999999999998897304E-05 ),
 .UNSPECIFIED. ) ;
#66345=ORIENTED_EDGE ( 'NONE', *, *, #1955, .F. ) ;
#66346=CARTESIAN_POINT ( 'NONE',  ( -80.51775687497260492, -25.31554036629395554, 4.968850436570557250 ) ) ;
#66348=B_SPLINE_SURFACE_WITH_KNOTS ( 'NONE', 3, 1, ( 
 ( #43124, #88804 ),
 ( #81683, #42636 ),
 ( #10672, #33504 ),
 ( #64490, #42142 ),
 ( #74073, #27398 ),
 ( #73574, #25893 ),
 ( #80181, #34012 ),
 ( #26397, #56866 ),
 ( #87797, #57369 ),
 ( #18770, #41634 ),
 ( #19269, #50240 ),
 ( #81180, #11658 ),
 ( #4062, #35007 ),
 ( #65987, #96904 ),
 ( #89294, #19763 ),
 ( #50739, #37501 ),
 ( #5051, #66972 ),
 ( #83164, #37000 ),
 ( #68454, #99391 ) ),
 .UNSPECIFIED., .F., .F., .F.,
 ( 4, 1, 1, 1, 1, 1, 1, 1, 1, 1, 1, 1, 1, 1, 1, 1, 4 ),
 ( 2, 2 ),
 ( 0.000000000000000000, 0.06629491280198847314, 0.1301311164811693732, 0.1928622251726082593, 0.2543600042042246101, 0.3159098460813289933, 0.3773381393463554612, 0.4402052628879283280, 0.5041751317708966784, 0.5680336324132717607, 0.6302277217668702525, 0.6908614774070669373, 0.7514218176484559475, 0.8114657367408623090, 0.8727504667961283324, 0.9353907348444668868, 1.000000000000000000 ),
 ( 0.000000000000000000, 1.000000000000000000 ),
 .UNSPECIFIED. ) ;
#66349=CARTESIAN_POINT ( 'NONE',  ( -78.62287095715007013, -23.95044443724992078, 10.65354141964649237 ) ) ;
#66351=CARTESIAN_POINT ( 'NONE',  ( -21.15187133135857422, -0.9709546189074961253, 11.49999999999998934 ) ) ;
#66352=CARTESIAN_POINT ( 'NONE',  ( -49.62287095715005592, -29.50250243563736774, 8.947779886222146928 ) ) ;
#66354=CARTESIAN_POINT ( 'NONE',  ( 22.30035941410032763, -0.3387204123245128873, -1.500000000000002220 ) ) ;
#66360=CARTESIAN_POINT ( 'NONE',  ( -83.62287095715005592, -24.64965695001468404, 8.947790433994182280 ) ) ;
#66361=CARTESIAN_POINT ( 'NONE',  ( -3.338044803349280443, -19.22079736023769669, -1.500000000000002220 ) ) ;
#66362=CARTESIAN_POINT ( 'NONE',  ( -13.24026558610970916, 16.85365899302435722, 11.49999999999998934 ) ) ;
#66364=DIRECTION ( 'NONE',  ( 3.773278334444167608E-23, -1.000000000000000000, 0.000000000000000000 ) ) ;
#66365=PLANE ( 'NONE',  #97643 ) ;
#66366=CARTESIAN_POINT ( 'NONE',  ( 7.682656365740156090, -21.48159684637525046, -1.500000000000002220 ) ) ;
#66367=EDGE_CURVE ( 'NONE', #55585, #15484, #7985, .T. ) ;
#66369=CARTESIAN_POINT ( 'NONE',  ( -106.5551925487616671, -23.96169478059714564, 10.65365249895717170 ) ) ;
#66370=CARTESIAN_POINT ( 'NONE',  ( -128.5228709571500758, -23.94994826722564696, -0.6494450866342721396 ) ) ;
#66371=CARTESIAN_POINT ( 'NONE',  ( -13.68957358570155769, -14.46295258127404892, 11.49999999999999645 ) ) ;
#66372=FACE_OUTER_BOUND ( 'NONE', #55803, .T. ) ;
#66374=CARTESIAN_POINT ( 'NONE',  ( -39.64153524556972741, -24.15620529776628089, 10.23563542870661180 ) ) ;
#66375=CARTESIAN_POINT ( 'NONE',  ( -98.58953762381672448, -23.47593901973091235, -1.443836447539001089 ) ) ;
#66376=EDGE_LOOP ( 'NONE', ( #26618, #41631, #24980, #59462 ) ) ;
#66377=B_SPLINE_CURVE_WITH_KNOTS ( 'NONE', 3,
 ( #92300, #30400, #21774, #5569 ),
 .UNSPECIFIED., .F., .F.,
 ( 4, 4 ),
 ( 0.000000000000000000, 9.999999999998900014E-05 ),
 .UNSPECIFIED. ) ;
#66378=FACE_OUTER_BOUND ( 'NONE', #23390, .T. ) ;
#66379=CARTESIAN_POINT ( 'NONE',  ( -32.42024351695030759, -24.87479601683088148, 8.247789944647561100 ) ) ;
#66380=CARTESIAN_POINT ( 'NONE',  ( 21.38347125639554136, -3.707035686939989638, 11.49999999999998934 ) ) ;
#66383=CARTESIAN_POINT ( 'NONE',  ( 16.94836550497923966, -9.742303593519430649, -1.500000000000002220 ) ) ;
#66389=CARTESIAN_POINT ( 'NONE',  ( -69.62287095715009855, -24.33927499327854704, 9.819080762295822495 ) ) ;
#66390=CARTESIAN_POINT ( 'NONE',  ( -12.74120943341865342, -16.01528480738631899, 11.49999999999999645 ) ) ;
#66392=B_SPLINE_CURVE_WITH_KNOTS ( 'NONE', 3,
 ( #66412, #90718, #13078, #97332, #65914, #21192, #27820, #58774, #98819, #5976, #75974, #52158, #98315, #89726 ),
 .UNSPECIFIED., .F., .F.,
 ( 4, 2, 2, 2, 2, 2, 4 ),
 ( 7.059813062317230268E-18, 0.0003111425035767722246, 0.0006222850071535374018, 0.0007778562589419200446, 0.0009334275107303025790, 0.001088998762518685222, 0.001244570014307067865 ),
 .UNSPECIFIED. ) ;
#66393=CARTESIAN_POINT ( 'NONE',  ( -86.58953762381672448, -24.64965694238406968, 8.947790433994656567 ) ) ;
#66395=AXIS2_PLACEMENT_3D ( 'NONE', #25999, #48350, #63078 ) ;
#66396=ORIENTED_EDGE ( 'NONE', *, *, #91821, .T. ) ;
#66402=ORIENTED_EDGE ( 'NONE', *, *, #74230, .T. ) ;
#66403=ADVANCED_FACE ( 'NONE', ( #70390 ), #86111, .F. ) ;
#66407=B_SPLINE_CURVE_WITH_KNOTS ( 'NONE', 3,
 ( #77941, #47024, #7948, #30791 ),
 .UNSPECIFIED., .F., .F.,
 ( 4, 4 ),
 ( 0.000000000000000000, 9.999999999998206125E-05 ),
 .UNSPECIFIED. ) ;
#66408=CARTESIAN_POINT ( 'NONE',  ( 17.37538969058663696, -15.08583811485692117, 11.49999999999999645 ) ) ;
#66409=CARTESIAN_POINT ( 'NONE',  ( -16.34568771794417685, -15.85656593008108750, -1.500000000000002220 ) ) ;
#66410=CARTESIAN_POINT ( 'NONE',  ( -110.5570691414250746, -23.85049219812686161, 10.88485053497526778 ) ) ;
#66412=CARTESIAN_POINT ( 'NONE',  ( -50.40445135320379677, -25.19502912051677868, 3.293943094755626078 ) ) ;
#66415=CARTESIAN_POINT ( 'NONE',  ( -70.32380231474228083, -25.13313949306887096, 7.101635536975467566 ) ) ;
#66416=CARTESIAN_POINT ( 'NONE',  ( -11.18773875818744656, -18.78983145652188469, -1.500000000000002220 ) ) ;
#66417=CARTESIAN_POINT ( 'NONE',  ( -31.52287095715006160, -24.65952944569304606, 1.056160979905690134 ) ) ;
#66418=DIRECTION ( 'NONE',  ( -3.773278334453079618E-23, 0.9999999999976377785, 2.173523156925979975E-06 ) ) ;
#66420=CARTESIAN_POINT ( 'NONE',  ( -48.52287095715007581, -23.47593901973090524, -1.443836447538997314 ) ) ;
#66422=CARTESIAN_POINT ( 'NONE',  ( 13.37706023731332827, -15.40713922116925616, 11.49999999999998934 ) ) ;
#66423=EDGE_LOOP ( 'NONE', ( #83358, #79522, #56832, #52105 ) ) ;
#66424=VERTEX_POINT ( 'NONE', #55683 ) ;
#66426=ORIENTED_EDGE ( 'NONE', *, *, #89465, .F. ) ;
#66427=ADVANCED_FACE ( 'NONE', ( #1884 ), #24703, .T. ) ;
#66429=CARTESIAN_POINT ( 'NONE',  ( -7.156825135384894843, 21.90021990432103038, -1.500000000000002220 ) ) ;
#66431=CARTESIAN_POINT ( 'NONE',  ( 7.037473118728134303, -18.94123407977296480, -1.500000000000002220 ) ) ;
#66433=CARTESIAN_POINT ( 'NONE',  ( -98.62287095715009855, -23.95044443724991012, 10.65354141964649592 ) ) ;
#66435=B_SPLINE_CURVE_WITH_KNOTS ( 'NONE', 3,
 ( #23658, #38893, #54631, #16048, #1348, #56140, #32283, #95188 ),
 .UNSPECIFIED., .F., .F.,
 ( 4, 2, 2, 4 ),
 ( -0.001224554619866351050, -0.0002241820295893694366, 0.0007761905606876121771, 0.002776935741241578874 ),
 .UNSPECIFIED. ) ;
#66437=DIRECTION ( 'NONE',  ( 0.000000000000000000, -0.9999999999976377785, -2.173523156925979975E-06 ) ) ;
#66438=CARTESIAN_POINT ( 'NONE',  ( -21.34312709018487553, 1.176582458498846462, 11.49999999999999645 ) ) ;
#66441=ORIENTED_EDGE ( 'NONE', *, *, #2828, .T. ) ;
#66442=CARTESIAN_POINT ( 'NONE',  ( -19.27636426328722763, -11.15942449563467775, 11.49999999999998934 ) ) ;
#66443=CARTESIAN_POINT ( 'NONE',  ( -13.01863806243235899, 16.06808769575019014, 11.49999999999998934 ) ) ;
#66444=AXIS2_PLACEMENT_3D ( 'NONE', #20023, #19022, #49998 ) ;
#66446=ORIENTED_EDGE ( 'NONE', *, *, #70764, .T. ) ;
#66447=EDGE_CURVE ( 'NONE', #55725, #49833, #71903, .T. ) ;
#66448=CARTESIAN_POINT ( 'NONE',  ( -113.5228709571500616, -24.65952944569304961, 1.056160979905704123 ) ) ;
#66449=ORIENTED_EDGE ( 'NONE', *, *, #75818, .F. ) ;
#66451=VECTOR ( 'NONE', #83346, 1000.000000000000227 ) ;
#66453=B_SPLINE_CURVE_WITH_KNOTS ( 'NONE', 3,
 ( #17975, #81870, #33703, #3763 ),
 .UNSPECIFIED., .F., .F.,
 ( 4, 4 ),
 ( 0.000000000000000000, 9.999999999998897304E-05 ),
 .UNSPECIFIED. ) ;
#66455=CARTESIAN_POINT ( 'NONE',  ( -20.92377055399060737, -0.003182555231893603818, -1.500000000000002220 ) ) ;
#66456=CARTESIAN_POINT ( 'NONE',  ( -13.81295463269534096, 17.03802364079049525, 11.49999999999999645 ) ) ;
#66457=ADVANCED_FACE ( 'NONE', ( #10484 ), #64306, .T. ) ;
#66459=CARTESIAN_POINT ( 'NONE',  ( -18.95691745938505335, -12.16397891629814865, -1.500000000000002220 ) ) ;
#66460=VECTOR ( 'NONE', #46973, 1000.000000000000114 ) ;
#66461=CARTESIAN_POINT ( 'NONE',  ( 13.96602909953038640, 15.60522523583095200, 11.49999999999998934 ) ) ;
#66462=ADVANCED_FACE ( 'NONE', ( #72902 ), #50063, .F. ) ;
#66463=CARTESIAN_POINT ( 'NONE',  ( -92.62357510551103701, -24.66019654487200441, 8.947790411086112172 ) ) ;
#66467=VERTEX_POINT ( 'NONE', #96234 ) ;
#66469=AXIS2_PLACEMENT_3D ( 'NONE', #41836, #86983, #55555 ) ;
#66470=ORIENTED_EDGE ( 'NONE', *, *, #33430, .F. ) ;
#66471=AXIS2_PLACEMENT_3D ( 'NONE', #55042, #91712, #47927 ) ;
#66473=CARTESIAN_POINT ( 'NONE',  ( -66.51586562461079666, -23.73766607897669800, -1.055555164236460897 ) ) ;
#66475=CARTESIAN_POINT ( 'NONE',  ( 17.68986881342592454, -12.14045624799103962, -1.500000000000002220 ) ) ;
#66477=CARTESIAN_POINT ( 'NONE',  ( -59.52287095715006870, -24.51283580621364067, 0.6167428607019767028 ) ) ;
#66478=ORIENTED_EDGE ( 'NONE', *, *, #93919, .F. ) ;
#66479=CARTESIAN_POINT ( 'NONE',  ( -20.42954818520503935, 5.180689535515515587, 11.49999999999998934 ) ) ;
#66480=CARTESIAN_POINT ( 'NONE',  ( -99.52764846858842418, -25.27419814425944011, 3.999772249604663710 ) ) ;
#66482=CARTESIAN_POINT ( 'NONE',  ( -87.62287095715007013, -23.73907113216990439, -1.053371485793227258 ) ) ;
#66483=B_SPLINE_CURVE_WITH_KNOTS ( 'NONE', 3,
 ( #82834, #75224, #90455, #84834, #67632, #6711 ),
 .UNSPECIFIED., .F., .F.,
 ( 4, 2, 4 ),
 ( 0.000000000000000000, 0.001380764517854769519, 0.002761529035709539039 ),
 .UNSPECIFIED. ) ;
#66484=CARTESIAN_POINT ( 'NONE',  ( -102.5228709571500758, -29.50250786944525672, 11.44777988621623166 ) ) ;
#66486=CARTESIAN_POINT ( 'NONE',  ( 22.05266032001784637, -1.487345182339283367, -1.500000000000002220 ) ) ;
#66487=CARTESIAN_POINT ( 'NONE',  ( -91.62287095715004170, -24.64898659630368627, 1.056161002820827921 ) ) ;
#66489=CARTESIAN_POINT ( 'NONE',  ( -60.62371844064301030, -25.00158670708909980, 2.256160236439220146 ) ) ;
#66490=CARTESIAN_POINT ( 'NONE',  ( -25.52711720098805870, -24.43591384941821332, 1.590605884330588360 ) ) ;
#66491=CARTESIAN_POINT ( 'NONE',  ( -63.52287095715004739, -24.51283580621364067, 0.6167428607019723730 ) ) ;
#66492=CARTESIAN_POINT ( 'NONE',  ( 17.14628872753620215, 12.71262973326862245, 11.49999999999998934 ) ) ;
#66493=DIRECTION ( 'NONE',  ( 1.000000000000000000, 3.773278334444166432E-23, 8.201307841325785021E-29 ) ) ;
#66494=LINE ( 'NONE', #20765, #62479 ) ;
#66495=B_SPLINE_CURVE_WITH_KNOTS ( 'NONE', 3,
 ( #78798, #78303, #93527, #24522 ),
 .UNSPECIFIED., .F., .F.,
 ( 4, 4 ),
 ( 2.176968243509707518E-15, 0.0001007173067907758126 ),
 .UNSPECIFIED. ) ;
#66497=CARTESIAN_POINT ( 'NONE',  ( -68.52287095715006160, -23.48783264082476308, -1.443836473390092356 ) ) ;
#66498=CARTESIAN_POINT ( 'NONE',  ( 22.31954755298990278, 3.869410565987296380, -1.500000000000002220 ) ) ;
#66499=DIRECTION ( 'NONE',  ( -1.000000000000000000, -3.773278334444166432E-23, -8.201307841325785021E-29 ) ) ;
#66500=ORIENTED_EDGE ( 'NONE', *, *, #84017, .F. ) ;
#66501=LINE ( 'NONE', #91299, #57980 ) ;
#66503=CARTESIAN_POINT ( 'NONE',  ( -16.05533900033903549, 11.45903963230415101, 11.49999999999999645 ) ) ;
#66505=CARTESIAN_POINT ( 'NONE',  ( -67.50570964152612419, -24.15543982623906416, -0.2315651400026651485 ) ) ;
#66506=ORIENTED_EDGE ( 'NONE', *, *, #12946, .T. ) ;
#66508=CARTESIAN_POINT ( 'NONE',  ( -110.5228709571500758, -23.47593901973090524, -1.443836447538996204 ) ) ;
#66510=CARTESIAN_POINT ( 'NONE',  ( -21.34238180412542718, 3.497892552127677135, 11.49999999999998934 ) ) ;
#66512=CARTESIAN_POINT ( 'NONE',  ( 14.52268490272241408, 12.84546865777419455, -1.500000000000002220 ) ) ;
#66513=CARTESIAN_POINT ( 'NONE',  ( -109.5895376238167245, -23.47593901973091235, -1.443836447538999312 ) ) ;
#66514=CARTESIAN_POINT ( 'NONE',  ( -80.59913673259377731, -25.04344369319006702, 7.561456861807408281 ) ) ;
#66515=CARTESIAN_POINT ( 'NONE',  ( -19.57314199983870751, -2.777824058246878280, 11.49999999999998934 ) ) ;
#66517=CARTESIAN_POINT ( 'NONE',  ( 19.35245777310151993, -6.127589836641541332, 11.49999999999999645 ) ) ;
#66518=PLANE ( 'NONE',  #44040 ) ;
#66521=EDGE_CURVE ( 'NONE', #82927, #53278, #26098, .T. ) ;
#66523=CARTESIAN_POINT ( 'NONE',  ( -37.52287095715006870, -23.48786465467240347, 11.44779295918255180 ) ) ;
#66524=CARTESIAN_POINT ( 'NONE',  ( -107.2228709571500644, -23.47596703998600631, 11.44779298504227860 ) ) ;
#66528=EDGE_CURVE ( 'NONE', #61101, #50459, #14048, .T. ) ;
#66529=CARTESIAN_POINT ( 'NONE',  ( -33.52287095715007581, -23.48783264083359512, -1.443836473376374441 ) ) ;
#66530=CARTESIAN_POINT ( 'NONE',  ( -15.86121933104946535, 12.22609501325904624, 11.49999999999998934 ) ) ;
#66531=EDGE_CURVE ( 'NONE', #93563, #72639, #86467, .T. ) ;
#66532=CARTESIAN_POINT ( 'NONE',  ( -67.52287095715009002, -23.48783264082477018, -1.443836473390090802 ) ) ;
#66533=EDGE_LOOP ( 'NONE', ( #25334, #82742, #1124, #61254 ) ) ;
#66539=DIRECTION ( 'NONE',  ( 0.000000000000000000, 0.9999999999976377785, 2.173523156925979128E-06 ) ) ;
#66543=VECTOR ( 'NONE', #18171, 1000.000000000000114 ) ;
#66544=FACE_OUTER_BOUND ( 'NONE', #76799, .T. ) ;
#66548=CARTESIAN_POINT ( 'NONE',  ( -17.48930418531667996, -10.34094407820366612, -1.500000000000002220 ) ) ;
#66549=ORIENTED_EDGE ( 'NONE', *, *, #7544, .T. ) ;
#66550=EDGE_CURVE ( 'NONE', #65344, #37472, #25709, .T. ) ;
#66551=CARTESIAN_POINT ( 'NONE',  ( 22.43992371924722917, 4.826111843257130829, 11.49999999999998934 ) ) ;
#66552=CARTESIAN_POINT ( 'NONE',  ( -32.64292742023518912, -24.15543982623907127, -0.2315651400026567941 ) ) ;
#66554=CARTESIAN_POINT ( 'NONE',  ( -49.56947780960053507, -25.30465585254130190, 4.839518961770515659 ) ) ;
#66556=ADVANCED_FACE ( 'NONE', ( #87620 ), #75871, .T. ) ;
#66558=CARTESIAN_POINT ( 'NONE',  ( -4.955175619359221351, 20.59750927568439138, 11.49999999999999645 ) ) ;
#66559=ORIENTED_EDGE ( 'NONE', *, *, #48525, .F. ) ;
#66560=CARTESIAN_POINT ( 'NONE',  ( 15.99899278244174639, -15.33069297701436184, -1.500000000000002220 ) ) ;
#66561=CARTESIAN_POINT ( 'NONE',  ( 19.39738937107077632, -6.937168198526852514, -1.500000000000002220 ) ) ;
#66562=ORIENTED_EDGE ( 'NONE', *, *, #38482, .T. ) ;
#66563=ORIENTED_EDGE ( 'NONE', *, *, #61110, .F. ) ;
#66564=CARTESIAN_POINT ( 'NONE',  ( -82.62287095715005592, -29.50250786944525672, 11.44777988621623521 ) ) ;
#66566=ORIENTED_EDGE ( 'NONE', *, *, #48557, .T. ) ;
#66567=ORIENTED_EDGE ( 'NONE', *, *, #20096, .F. ) ;
#66568=ORIENTED_EDGE ( 'NONE', *, *, #10614, .T. ) ;
#66569=PLANE ( 'NONE',  #12950 ) ;
#66570=CARTESIAN_POINT ( 'NONE',  ( -71.58953762381672448, -24.64965694238407323, 8.947790433994656567 ) ) ;
#66572=CARTESIAN_POINT ( 'NONE',  ( 14.12806351585482112, -15.20395780304818523, -1.500000000000002220 ) ) ;
#66573=CARTESIAN_POINT ( 'NONE',  ( 3.708801897538985148, -21.39311272803122321, 11.49999999999999645 ) ) ;
#66575=CARTESIAN_POINT ( 'NONE',  ( -121.9228709571500957, -23.47593901973090524, -1.443836447538996204 ) ) ;
#66576=CARTESIAN_POINT ( 'NONE',  ( -119.6228709571500701, -23.48786465467241769, 11.44779295918253759 ) ) ;
#66577=CARTESIAN_POINT ( 'NONE',  ( -20.53624283083718893, 9.024085183690161216, -1.500000000000002220 ) ) ;
#66579=CARTESIAN_POINT ( 'NONE',  ( -93.22287095715005023, -23.47593901973090524, -1.443836447538996870 ) ) ;
#66580=CARTESIAN_POINT ( 'NONE',  ( -65.63298288181091777, -24.63355581998386867, 0.9682620441943842193 ) ) ;
#66581=ORIENTED_EDGE ( 'NONE', *, *, #10198, .T. ) ;
#66582=CARTESIAN_POINT ( 'NONE',  ( -59.52287095715005449, -24.50321055353803601, 9.387540953477529371 ) ) ;
#66583=CARTESIAN_POINT ( 'NONE',  ( -89.81226385320383088, -25.05712135967894838, 7.447789548357302891 ) ) ;
#66584=ORIENTED_EDGE ( 'NONE', *, *, #89968, .T. ) ;
#66586=AXIS2_PLACEMENT_3D ( 'NONE', #86392, #1666, #10776 ) ;
#66587=ADVANCED_FACE ( 'NONE', ( #83989 ), #27990, .T. ) ;
#66588=CARTESIAN_POINT ( 'NONE',  ( -75.52287095715007581, -29.50247984919015209, -1.443849546365053582 ) ) ;
#66589=ORIENTED_EDGE ( 'NONE', *, *, #85284, .F. ) ;
#66590=CARTESIAN_POINT ( 'NONE',  ( -13.45305159987462851, 16.49040971879131234, -1.500000000000002220 ) ) ;
#66591=ORIENTED_EDGE ( 'NONE', *, *, #23659, .F. ) ;
#66592=CARTESIAN_POINT ( 'NONE',  ( -101.0861487085838206, -25.15054751950415124, 6.938118937714361500 ) ) ;
#66593=CARTESIAN_POINT ( 'NONE',  ( 19.95399986947220583, -8.914707708046476498, 11.49999999999998934 ) ) ;
#66594=CARTESIAN_POINT ( 'NONE',  ( -51.04357394935764347, -25.30543060587211812, 4.940877950953177056 ) ) ;
#66595=CARTESIAN_POINT ( 'NONE',  ( 20.21490908150494192, 10.32750977814155391, 11.49999999999998934 ) ) ;
#66596=CARTESIAN_POINT ( 'NONE',  ( -41.01720553446741491, -25.18430903175909208, 3.440463593108834317 ) ) ;
#66598=CARTESIAN_POINT ( 'NONE',  ( -5.132426408838210108, -21.30661980433056968, -1.500000000000002220 ) ) ;
#66599=LINE ( 'NONE', #27515, #59282 ) ;
#66600=ORIENTED_EDGE ( 'NONE', *, *, #40417, .F. ) ;
#66602=DIRECTION ( 'NONE',  ( 3.773278334444167608E-23, -1.000000000000000000, 0.000000000000000000 ) ) ;
#66603=VERTEX_POINT ( 'NONE', #37819 ) ;
#66604=CARTESIAN_POINT ( 'NONE',  ( -32.52287095715006870, -24.50321055353803956, 9.387540953477529371 ) ) ;
#66606=CARTESIAN_POINT ( 'NONE',  ( -40.94688081444584782, -25.03284417894045788, 7.563176522466704910 ) ) ;
#66608=CARTESIAN_POINT ( 'NONE',  ( -20.43227410087897056, -23.69217786884635402, 0.5637492489085929037 ) ) ;
#66609=CARTESIAN_POINT ( 'NONE',  ( -4.916304867406160461, -20.68799595667769964, 11.49999999999998934 ) ) ;
#66610=CARTESIAN_POINT ( 'NONE',  ( -112.5204660179142024, -23.73766607897671577, -1.055555164236427368 ) ) ;
#66611=DIRECTION ( 'NONE',  ( -3.773278334453080206E-23, 0.9999999999976377785, 2.173523156925979975E-06 ) ) ;
#66614=CARTESIAN_POINT ( 'NONE',  ( -84.52287095715006160, -23.48786465467241769, 11.44779295918254469 ) ) ;
#66615=ORIENTED_EDGE ( 'NONE', *, *, #996, .T. ) ;
#66616=CARTESIAN_POINT ( 'NONE',  ( 16.73968668634701729, 10.17700309559984717, 11.49999999999999645 ) ) ;
#66617=CARTESIAN_POINT ( 'NONE',  ( -58.62287095715003460, -23.73934037231756378, 11.05740245334329153 ) ) ;
#66618=CARTESIAN_POINT ( 'NONE',  ( -68.62287095715005592, -24.64898659630367916, 1.056161002820824368 ) ) ;
#66619=VERTEX_POINT ( 'NONE', #21578 ) ;
#66621=CARTESIAN_POINT ( 'NONE',  ( -85.52287095715009002, -23.47593901973090524, -1.443836447538996648 ) ) ;
#66622=CARTESIAN_POINT ( 'NONE',  ( -122.6228709571500417, -23.47593901973091235, -1.443836447538997536 ) ) ;
#66623=B_SPLINE_CURVE_WITH_KNOTS ( 'NONE', 3,
 ( #14738, #82756, #7131, #5138, #67061, #97969, #44212, #71214, #78799, #53995, #63618, #193, #9297, #76795 ),
 .UNSPECIFIED., .F., .F.,
 ( 4, 2, 2, 2, 2, 2, 4 ),
 ( 1.411962612463446054E-17, 0.0001548496297124576687, 0.0003096992594249011886, 0.0006193985188498282897, 0.0007742481485622923010, 0.0009290977782747563123, 0.001238797037699685202 ),
 .UNSPECIFIED. ) ;
#66624=CARTESIAN_POINT ( 'NONE',  ( -106.5228709571500332, -23.48783264082477018, -1.443836473390085695 ) ) ;
#66625=CARTESIAN_POINT ( 'NONE',  ( -9.385407830382300531, 17.29636241635495608, 11.49999999999998934 ) ) ;
#66627=DIRECTION ( 'NONE',  ( -3.773278334453079030E-23, 0.9999999999976377785, 2.173523156925979128E-06 ) ) ;
#66628=DIRECTION ( 'NONE',  ( 3.773278334444167608E-23, -1.000000000000000000, 0.000000000000000000 ) ) ;
#66631=VERTEX_POINT ( 'NONE', #53560 ) ;
#66634=CARTESIAN_POINT ( 'NONE',  ( -47.60694479324835271, -23.73766607897670866, -1.055555164236438914 ) ) ;
#66635=DIRECTION ( 'NONE',  ( -3.773278334444166432E-23, 1.000000000000000000, 0.000000000000000000 ) ) ;
#66636=CARTESIAN_POINT ( 'NONE',  ( -115.6228709571500559, -23.47596703998600631, 11.44779298504227860 ) ) ;
#66638=CARTESIAN_POINT ( 'NONE',  ( -31.52166505407126706, -24.86441978397624553, 8.247789967200544581 ) ) ;
#66639=B_SPLINE_CURVE_WITH_KNOTS ( 'NONE', 3,
 ( #40831, #57080, #72294, #88015 ),
 .UNSPECIFIED., .F., .F.,
 ( 4, 4 ),
 ( 0.000000000000000000, 9.999999999998897304E-05 ),
 .UNSPECIFIED. ) ;
#66641=CARTESIAN_POINT ( 'NONE',  ( -8.813339738934139689, -17.91118242276673911, 11.49999999999998934 ) ) ;
#66642=ADVANCED_FACE ( 'NONE', ( #76853 ), #35828, .F. ) ;
#66643=CARTESIAN_POINT ( 'NONE',  ( -41.62287095715006302, -24.66019654487199020, 8.947790411086135265 ) ) ;
#66644=CARTESIAN_POINT ( 'NONE',  ( -0.003591441230561016797, -23.00350597096012351, 6.154653013508758264 ) ) ;
#66645=EDGE_LOOP ( 'NONE', ( #60431, #59289, #42946, #36746 ) ) ;
#66646=CARTESIAN_POINT ( 'NONE',  ( -117.5228709571500758, -29.50250786944525672, 11.44777988621622811 ) ) ;
#66649=EDGE_CURVE ( 'NONE', #81670, #13730, #24829, .T. ) ;
#66652=CARTESIAN_POINT ( 'NONE',  ( -126.7286271109977775, -25.23514665191783735, 6.311484830854977801 ) ) ;
#66656=CARTESIAN_POINT ( 'NONE',  ( -26.09636659181000340, -24.96935267319560126, 4.940287552382958580 ) ) ;
#66662=CARTESIAN_POINT ( 'NONE',  ( 14.48468284575590204, 14.13777120147990729, 11.49999999999998934 ) ) ;
#66663=CARTESIAN_POINT ( 'NONE',  ( -122.6256512063165189, -23.96119346886880663, -0.6495511937832028071 ) ) ;
#66664=CARTESIAN_POINT ( 'NONE',  ( -129.6228709571498996, -24.33832256527048798, 0.1851278514138701703 ) ) ;
#66666=ORIENTED_EDGE ( 'NONE', *, *, #8092, .F. ) ;
#66668=DIRECTION ( 'NONE',  ( 0.000000000000000000, -2.173523156925980399E-06, 0.9999999999976378895 ) ) ;
#66670=CARTESIAN_POINT ( 'NONE',  ( 0.1258803491696451060, 20.03332480481931199, -1.500000000000002220 ) ) ;
#66671=B_SPLINE_CURVE_WITH_KNOTS ( 'NONE', 3,
 ( #69067, #557, #46741, #16781 ),
 .UNSPECIFIED., .F., .F.,
 ( 4, 4 ),
 ( 0.000000000000000000, 0.0001002978978731602401 ),
 .UNSPECIFIED. ) ;
#66672=CARTESIAN_POINT ( 'NONE',  ( 20.75205275252385206, -3.532026382766447536, 11.49999999999999645 ) ) ;
#66674=CARTESIAN_POINT ( 'NONE',  ( -27.97342827235127061, -24.83868590882142868, 7.574733681428329923 ) ) ;
#66675=CARTESIAN_POINT ( 'NONE',  ( -111.6228709571500843, -23.95044443724992433, 10.65354141964650481 ) ) ;
#66676=CARTESIAN_POINT ( 'NONE',  ( -4.445301477617020325, 21.63612927058290936, -1.500000000000002220 ) ) ;
#66677=B_SPLINE_CURVE_WITH_KNOTS ( 'NONE', 3,
 ( #3544, #49727, #42116, #9139 ),
 .UNSPECIFIED., .F., .F.,
 ( 4, 4 ),
 ( 2.830056797201531266E-06, 0.0004722118875754793095 ),
 .UNSPECIFIED. ) ;
#66678=CARTESIAN_POINT ( 'NONE',  ( -39.85544541354917669, -25.27806075124410157, 4.937103068824292507 ) ) ;
#66680=CARTESIAN_POINT ( 'NONE',  ( -50.40445135320380388, -25.18440101920884189, 3.293943117856050762 ) ) ;
#66681=VERTEX_POINT ( 'NONE', #94598 ) ;
#66682=CARTESIAN_POINT ( 'NONE',  ( -35.52287095715008292, -25.00182538069144655, 7.747789668545105535 ) ) ;
#66683=CARTESIAN_POINT ( 'NONE',  ( -31.60165242513933492, -23.96119346886880663, -0.6495511937832003646 ) ) ;
#66684=ORIENTED_EDGE ( 'NONE', *, *, #59236, .F. ) ;
#66685=ORIENTED_EDGE ( 'NONE', *, *, #3045, .F. ) ;
#66688=CARTESIAN_POINT ( 'NONE',  ( -76.60617745381290433, -23.48783264082477373, -1.443836473390089026 ) ) ;
#66689=CARTESIAN_POINT ( 'NONE',  ( -0.003042231299257275486, -20.61035990087709635, -1.500000000000002220 ) ) ;
#66690=CARTESIAN_POINT ( 'NONE',  ( -8.857468890034409625, -19.66367526556523870, 11.49999999999999645 ) ) ;
#66691=EDGE_LOOP ( 'NONE', ( #38671, #40035, #19425, #6733 ) ) ;
#66692=CARTESIAN_POINT ( 'NONE',  ( -83.62287095715008434, -23.72773821059536559, 11.05748984161097503 ) ) ;
#66693=LINE ( 'NONE', #60563, #95275 ) ;
#66694=CARTESIAN_POINT ( 'NONE',  ( -114.6228709571500559, -29.50250786944525672, 11.44777988621622988 ) ) ;
#66695=CARTESIAN_POINT ( 'NONE',  ( 16.92800457317958518, -14.60656088873787262, 11.49999999999998934 ) ) ;
#66698=ORIENTED_EDGE ( 'NONE', *, *, #43043, .F. ) ;
#66699=CARTESIAN_POINT ( 'NONE',  ( -94.52287095715011844, -23.48783264082477373, -1.443836473390087027 ) ) ;
#66701=CARTESIAN_POINT ( 'NONE',  ( 12.60132613692001691, 16.66296579206088069, 11.49999999999998934 ) ) ;
#66703=ADVANCED_FACE ( 'NONE', ( #55553 ), #25079, .F. ) ;
#66704=CARTESIAN_POINT ( 'NONE',  ( -39.18367763993130382, -25.22434093780323394, 3.596805738460790547 ) ) ;
#66705=VERTEX_POINT ( 'NONE', #55049 ) ;
#66707=CARTESIAN_POINT ( 'NONE',  ( -100.6369782943210254, -23.85049219812686161, 10.88485053497527133 ) ) ;
#66708=CARTESIAN_POINT ( 'NONE',  ( -16.97324839047195866, 12.58421825509937442, -1.500000000000002220 ) ) ;
#66709=ADVANCED_FACE ( 'NONE', ( #61673 ), #54543, .F. ) ;
#66711=CARTESIAN_POINT ( 'NONE',  ( -96.22287095715009286, -23.47593901973090524, -1.443836447538997314 ) ) ;
#66713=PLANE ( 'NONE',  #5965 ) ;
#66714=CARTESIAN_POINT ( 'NONE',  ( -68.52287095715006160, -23.48786465467241058, 11.44779295918254647 ) ) ;
#66716=CARTESIAN_POINT ( 'NONE',  ( -21.05831370385527990, 5.553659732266172711, -1.500000000000002220 ) ) ;
#66718=CARTESIAN_POINT ( 'NONE',  ( -21.99995728619510516, 3.820703864638951952, 11.49999999999999645 ) ) ;
#66719=VERTEX_POINT ( 'NONE', #70768 ) ;
#66720=CARTESIAN_POINT ( 'NONE',  ( -45.62287095715004881, -25.00158670708908915, 2.256160236439166855 ) ) ;
#66721=CARTESIAN_POINT ( 'NONE',  ( -97.62287095715005592, -24.66019654487200086, 8.947790411086124607 ) ) ;
#66724=CARTESIAN_POINT ( 'NONE',  ( -56.62287095715005592, -23.48783264082478084, -1.443836473390068820 ) ) ;
#66726=ORIENTED_EDGE ( 'NONE', *, *, #85655, .F. ) ;
#66727=LINE ( 'NONE', #4309, #1088 ) ;
#66731=CARTESIAN_POINT ( 'NONE',  ( -49.17860766247945747, -25.30062163087967519, 4.391665315653317414 ) ) ;
#66735=CARTESIAN_POINT ( 'NONE',  ( -19.00951991574052968, 3.723548053296564575, 11.49999999999999645 ) ) ;
#66736=CARTESIAN_POINT ( 'NONE',  ( -115.5228709571500048, -24.15516710230294350, 10.28746687063725851 ) ) ;
#66737=EDGE_LOOP ( 'NONE', ( #58785, #71828, #95858, #2881 ) ) ;
#66740=DIRECTION ( 'NONE',  ( -1.000000000000000000, -3.773278334444167608E-23, -8.201307833595939069E-29 ) ) ;
#66741=CARTESIAN_POINT ( 'NONE',  ( -30.63240354163743717, -23.78087380709146004, 10.97511746239721298 ) ) ;
#66743=CARTESIAN_POINT ( 'NONE',  ( 5.347671334029483248, -18.86178030415664963, -1.500000000000002220 ) ) ;
#66744=CARTESIAN_POINT ( 'NONE',  ( -116.6228709571500559, -24.65952944569305316, 1.056160979905706121 ) ) ;
#66746=VERTEX_POINT ( 'NONE', #77856 ) ;
#66747=CARTESIAN_POINT ( 'NONE',  ( -4.138935798035190849, -21.16376344109877294, -1.500000000000002220 ) ) ;
#66748=CARTESIAN_POINT ( 'NONE',  ( -33.53806327265973408, -24.35071581493542325, 9.817618358456039473 ) ) ;
#66749=CARTESIAN_POINT ( 'NONE',  ( -81.14580165399679856, -25.30394787373862187, 5.096590184867776152 ) ) ;
#66750=CARTESIAN_POINT ( 'NONE',  ( -40.62513263387344864, -23.48783264082477018, -1.443836473390102570 ) ) ;
#66752=CARTESIAN_POINT ( 'NONE',  ( -19.99251892732797486, -11.32171818645973538, -1.500000000000002220 ) ) ;
#66756=CARTESIAN_POINT ( 'NONE',  ( 16.24926901856429140, 11.90123039513101411, 11.49999999999999645 ) ) ;
#66758=CARTESIAN_POINT ( 'NONE',  ( -32.51245690601021465, -23.73791477778911485, 11.05961554403171299 ) ) ;
#66759=PLANE ( 'NONE',  #11705 ) ;
#66760=CARTESIAN_POINT ( 'NONE',  ( -126.5228709571500616, -23.47596703998600631, 11.44779298504227683 ) ) ;
#66761=CARTESIAN_POINT ( 'NONE',  ( -95.92287095715005307, -23.47596703998600276, 11.44779298504227860 ) ) ;
#66762=CARTESIAN_POINT ( 'NONE',  ( -7.150643268323968904, -18.52920452239153448, 11.49999999999998934 ) ) ;
#66763=B_SPLINE_CURVE_WITH_KNOTS ( 'NONE', 3,
 ( #80093, #47657, #80591, #40544 ),
 .UNSPECIFIED., .F., .F.,
 ( 4, 4 ),
 ( 0.000000000000000000, 0.0001000000000000167422 ),
 .UNSPECIFIED. ) ;
#66766=CARTESIAN_POINT ( 'NONE',  ( 6.578723047037327909, -18.57437435983987584, -1.500000000000002220 ) ) ;
#66767=CARTESIAN_POINT ( 'NONE',  ( -126.5204122989497222, -24.66019654487200796, 8.947790411086103290 ) ) ;
#66769=EDGE_CURVE ( 'NONE', #38340, #35617, #27183, .T. ) ;
#66770=LINE ( 'NONE', #97688, #30557 ) ;
#66772=CARTESIAN_POINT ( 'NONE',  ( 7.914317726235799100, 19.11507755054979896, 11.49999999999999645 ) ) ;
#66776=CARTESIAN_POINT ( 'NONE',  ( -16.57510365746454184, 15.48777146884464884, 11.49999999999999645 ) ) ;
#66779=DIRECTION ( 'NONE',  ( -3.773278334453079618E-23, 0.9999999999976377785, 2.173523156925979975E-06 ) ) ;
#66781=ADVANCED_FACE ( 'NONE', ( #32193 ), #1264, .F. ) ;
#66782=CARTESIAN_POINT ( 'NONE',  ( -36.62287095715006302, -24.65952944569303895, 1.056160979905693909 ) ) ;
#66784=ORIENTED_EDGE ( 'NONE', *, *, #15121, .T. ) ;
#66785=VERTEX_POINT ( 'NONE', #78857 ) ;
#66787=CARTESIAN_POINT ( 'NONE',  ( -15.36296916364455711, -16.94538937337987150, 11.49999999999998934 ) ) ;
#66788=LINE ( 'NONE', #51048, #81068 ) ;
#66789=CARTESIAN_POINT ( 'NONE',  ( -0.8629811567608781653, -21.54619324973139172, -1.500000000000002220 ) ) ;
#66790=CARTESIAN_POINT ( 'NONE',  ( -113.5917734516337561, -23.96169478059713853, 10.65365249895717348 ) ) ;
#66791=DIRECTION ( 'NONE',  ( 1.000000000000000000, 3.773278334444167608E-23, 8.201307833595939069E-29 ) ) ;
#66792=CARTESIAN_POINT ( 'NONE',  ( 21.78986343443989071, 5.811249688775594002, 11.49999999999999645 ) ) ;
#66795=CARTESIAN_POINT ( 'NONE',  ( 5.346615758220810477, 21.33151429383102382, 11.49999999999998934 ) ) ;
#66796=CARTESIAN_POINT ( 'NONE',  ( -111.5553612508262376, -23.96119346886881019, -0.6495511937832035843 ) ) ;
#66800=CARTESIAN_POINT ( 'NONE',  ( -49.62287095715005592, -29.50248528299804818, 1.056150453629033370 ) ) ;
#66801=ORIENTED_EDGE ( 'NONE', *, *, #794, .T. ) ;
#66802=CARTESIAN_POINT ( 'NONE',  ( -84.62287095715005592, -23.47593901973091235, -1.443836447539004642 ) ) ;
#66807=CARTESIAN_POINT ( 'NONE',  ( -103.5228709571501042, -23.47593901973090524, -1.443836447538996204 ) ) ;
#66808=CARTESIAN_POINT ( 'NONE',  ( -6.584652030910324250, 19.34213596296284265, -1.500000000000002220 ) ) ;
#66809=ORIENTED_EDGE ( 'NONE', *, *, #92720, .F. ) ;
#66810=CARTESIAN_POINT ( 'NONE',  ( -71.70841769935766763, -25.24715640642683923, 6.192981443001071895 ) ) ;
#66814=FACE_OUTER_BOUND ( 'NONE', #16329, .T. ) ;
#66816=ORIENTED_EDGE ( 'NONE', *, *, #3327, .T. ) ;
#66817=CARTESIAN_POINT ( 'NONE',  ( -50.52287095715006160, -23.47596703998600631, 11.44779298504229104 ) ) ;
#66818=CARTESIAN_POINT ( 'NONE',  ( -97.58953762381671027, -24.66019654487199730, 8.947790411086122830 ) ) ;
#66820=ORIENTED_EDGE ( 'NONE', *, *, #39416, .T. ) ;
#66821=CARTESIAN_POINT ( 'NONE',  ( 2.677173591928626806, -20.63698567995287902, -1.500000000000002220 ) ) ;
#66822=ORIENTED_EDGE ( 'NONE', *, *, #43649, .T. ) ;
#66826=CARTESIAN_POINT ( 'NONE',  ( -44.58953762381671737, -23.47596703998600276, 11.44779298504227505 ) ) ;
#66827=CARTESIAN_POINT ( 'NONE',  ( -33.52287095715007581, -23.94994826722564696, -0.6494450866342740269 ) ) ;
#66828=EDGE_LOOP ( 'NONE', ( #83406, #65051, #25655, #83209 ) ) ;
#66830=CARTESIAN_POINT ( 'NONE',  ( -114.6228709571500701, -23.73907113216991860, -1.053371485793227480 ) ) ;
#66833=CARTESIAN_POINT ( 'NONE',  ( -70.90175588921343319, -25.31201622164140019, 5.458926420340825203 ) ) ;
#66834=CARTESIAN_POINT ( 'NONE',  ( -8.753671783739276790, -20.25744411100385634, 11.49999999999999645 ) ) ;
#66835=ORIENTED_EDGE ( 'NONE', *, *, #67835, .F. ) ;
#66836=CARTESIAN_POINT ( 'NONE',  ( -72.62287095715008434, -24.51283580621364067, 0.6167428607019815878 ) ) ;
#66837=CARTESIAN_POINT ( 'NONE',  ( 22.41689761077644860, -2.907977976681301424, -1.500000000000002220 ) ) ;
#66838=LINE ( 'NONE', #59717, #11740 ) ;
#66840=VERTEX_POINT ( 'NONE', #71269 ) ;
#66844=CARTESIAN_POINT ( 'NONE',  ( -57.49752954236778635, -24.35071581493543036, 9.817618358456028815 ) ) ;
#66845=ORIENTED_EDGE ( 'NONE', *, *, #100353, .F. ) ;
#66847=CARTESIAN_POINT ( 'NONE',  ( -20.55991158545366204, 8.586518200734140294, -1.500000000000002220 ) ) ;
#66848=B_SPLINE_CURVE_WITH_KNOTS ( 'NONE', 3,
 ( #24433, #93437, #85327, #54899, #91946, #7709 ),
 .UNSPECIFIED., .F., .F.,
 ( 4, 2, 4 ),
 ( 6.391158118959991367E-06, 0.001387004593080781592, 0.002767618028042603297 ),
 .UNSPECIFIED. ) ;
#66849=CARTESIAN_POINT ( 'NONE',  ( -45.52287095715006160, -29.50247984919015209, -1.443849546365058689 ) ) ;
#66850=ORIENTED_EDGE ( 'NONE', *, *, #3275, .T. ) ;
#66854=CARTESIAN_POINT ( 'NONE',  ( -49.58953762381673158, -24.66019654487199020, 8.947790411086131712 ) ) ;
#66855=CARTESIAN_POINT ( 'NONE',  ( -11.52932745282126703, -15.74164922852205173, 11.49999999999998934 ) ) ;
#66857=CARTESIAN_POINT ( 'NONE',  ( -7.526967427842778946, 20.06989004931119425, -1.500000000000002220 ) ) ;
#66860=CARTESIAN_POINT ( 'NONE',  ( -52.62287095715005592, -24.64965695001467694, 8.947790433994185832 ) ) ;
#66861=CARTESIAN_POINT ( 'NONE',  ( -15.12447472116105729, 17.10960193589383849, -1.500000000000002220 ) ) ;
#66864=CARTESIAN_POINT ( 'NONE',  ( -7.409219584043468920, -18.53548363135739052, 11.49999999999999645 ) ) ;
#66865=CARTESIAN_POINT ( 'NONE',  ( -69.52287095715007581, -24.34917612406836440, 0.1852690917426526862 ) ) ;
#66866=CARTESIAN_POINT ( 'NONE',  ( -57.62287095715004881, -24.64898659630367916, 1.056161002820822592 ) ) ;
#66867=CARTESIAN_POINT ( 'NONE',  ( -48.56040139242229969, -23.73766607897670866, -1.055555164236436028 ) ) ;
#66870=CARTESIAN_POINT ( 'NONE',  ( -25.53098197642538736, -24.92569209777881056, 4.942811685741776984 ) ) ;
#66872=CARTESIAN_POINT ( 'NONE',  ( 0.4029737066630413311, -21.70969715354747009, 11.49999999999998934 ) ) ;
#66874=CARTESIAN_POINT ( 'NONE',  ( -9.627943313441900131, 16.98966435471970726, -1.500000000000002220 ) ) ;
#66875=CARTESIAN_POINT ( 'NONE',  ( -34.52287095715005449, -24.34917612407030063, 0.1852690917476900179 ) ) ;
#66876=AXIS2_PLACEMENT_3D ( 'NONE', #68831, #46489, #37385 ) ;
#66877=VERTEX_POINT ( 'NONE', #62166 ) ;
#66882=CARTESIAN_POINT ( 'NONE',  ( -12.12210191164509965, 16.44476101713275185, 11.49999999999999645 ) ) ;
#66883=CARTESIAN_POINT ( 'NONE',  ( -47.52287095715005449, -24.35013146730202749, 9.818937971375104823 ) ) ;
#66884=ADVANCED_FACE ( 'NONE', ( #26597 ), #91207, .T. ) ;
#66889=LINE ( 'NONE', #12071, #86581 ) ;
#66894=ORIENTED_EDGE ( 'NONE', *, *, #41886, .T. ) ;
#66896=B_SPLINE_CURVE_WITH_KNOTS ( 'NONE', 3,
 ( #29729, #273, #68298, #45471, #92121, #36852 ),
 .UNSPECIFIED., .F., .F.,
 ( 4, 2, 4 ),
 ( 0.000000000000000000, 0.001380764517853247083, 0.002761529035706494165 ),
 .UNSPECIFIED. ) ;
#66897=CARTESIAN_POINT ( 'NONE',  ( 20.85440106035463970, 9.703512019146668166, 11.49999999999999645 ) ) ;
#66898=CARTESIAN_POINT ( 'NONE',  ( -9.230423729802735622, -20.81519635545753033, -1.500000000000002220 ) ) ;
#66900=B_SPLINE_SURFACE_WITH_KNOTS ( 'NONE', 3, 3, ( 
 ( #20124, #5402, #51086, #28741 ),
 ( #11161, #73567, #4057, #65479 ),
 ( #78775, #35001, #86406, #24501 ),
 ( #57860, #50235, #97398, #12653 ),
 ( #80673, #65981, #96899, #26391 ),
 ( #81172, #42136, #42629, #49747 ),
 ( #73076, #3561, #43617, #55469 ) ),
 .UNSPECIFIED., .F., .F., .F.,
 ( 4, 3, 4 ),
 ( 4, 4 ),
 ( 0.7945040050992239200, 0.8970133687736496775, 0.9995227324480754350 ),
 ( 0.009496410415874824429, 0.01051351914406330537 ),
 .UNSPECIFIED. ) ;
#66901=CARTESIAN_POINT ( 'NONE',  ( -122.6228709571500417, -24.64898659630368627, 1.056161002820833028 ) ) ;
#66902=CARTESIAN_POINT ( 'NONE',  ( -120.5228709571500474, -24.62285846331434058, 9.038163153548365969 ) ) ;
#66904=CARTESIAN_POINT ( 'NONE',  ( -110.5858259164890569, -25.00158670708910336, 2.256160236439218814 ) ) ;
#66905=CARTESIAN_POINT ( 'NONE',  ( 21.76694381678408519, 2.417257996116004115, 11.49999999999998934 ) ) ;
#66906=LINE ( 'NONE', #89731, #88333 ) ;
#66908=CARTESIAN_POINT ( 'NONE',  ( -103.5562042904834072, -24.66019654487199730, 8.947790411086124607 ) ) ;
#66912=CARTESIAN_POINT ( 'NONE',  ( 19.60162835767302880, 5.811842276320244416, 11.49999999999998934 ) ) ;
#66914=ORIENTED_EDGE ( 'NONE', *, *, #46979, .T. ) ;
#66915=ORIENTED_EDGE ( 'NONE', *, *, #73619, .T. ) ;
#66916=VERTEX_POINT ( 'NONE', #58548 ) ;
#66917=EDGE_CURVE ( 'NONE', #85527, #10916, #28422, .T. ) ;
#66918=CARTESIAN_POINT ( 'NONE',  ( -11.96207688724106610, 19.68918167733909641, 11.49999999999998934 ) ) ;
#66919=CARTESIAN_POINT ( 'NONE',  ( -61.53495354322418365, -24.65952944569304606, 1.056160979905699682 ) ) ;
#66920=CARTESIAN_POINT ( 'NONE',  ( -13.29518446780263119, -15.22762515321373478, -1.500000000000002220 ) ) ;
#66921=VECTOR ( 'NONE', #22214, 1000.000000000000114 ) ;
#66922=VERTEX_POINT ( 'NONE', #81376 ) ;
#66923=FACE_OUTER_BOUND ( 'NONE', #13476, .T. ) ;
#66924=CARTESIAN_POINT ( 'NONE',  ( -127.5562042904833646, -24.64965694238575722, 8.947790433994185832 ) ) ;
#66925=CARTESIAN_POINT ( 'NONE',  ( -95.58393195655612828, -24.92564183028979841, 1.928384488918254425 ) ) ;
#66926=CARTESIAN_POINT ( 'NONE',  ( -53.65128113065046733, -23.73791477778911485, 11.05961554403170766 ) ) ;
#66927=CARTESIAN_POINT ( 'NONE',  ( 11.41860910855227829, 18.14899599152127152, 11.49999999999999645 ) ) ;
#66929=CARTESIAN_POINT ( 'NONE',  ( -113.6228709571500559, -23.47593901973091235, -1.443836447538999312 ) ) ;
#66931=VERTEX_POINT ( 'NONE', #10361 ) ;
#66932=CARTESIAN_POINT ( 'NONE',  ( 15.88595335714125589, -15.59144682577495189, 11.49999999999998934 ) ) ;
#66933=CARTESIAN_POINT ( 'NONE',  ( -1.398219401198234957, 20.63772364298462847, 11.49999999999998934 ) ) ;
#66934=ORIENTED_EDGE ( 'NONE', *, *, #92479, .T. ) ;
#66935=EDGE_CURVE ( 'NONE', #68864, #99512, #87743, .T. ) ;
#66936=CARTESIAN_POINT ( 'NONE',  ( -29.58953762381671382, -24.58200030392595892, 8.947790445854003849 ) ) ;
#66937=EDGE_LOOP ( 'NONE', ( #87234, #16606, #58667, #32681 ) ) ;
#66938=B_SPLINE_CURVE_WITH_KNOTS ( 'NONE', 3,
 ( #31648, #99645, #701, #60630 ),
 .UNSPECIFIED., .F., .F.,
 ( 4, 4 ),
 ( 0.4390812836509193628, 0.4400820306916847779 ),
 .UNSPECIFIED. ) ;
#66941=CARTESIAN_POINT ( 'NONE',  ( -16.12721948686093754, -13.32240427740599564, -1.500000000000002220 ) ) ;
#66942=CARTESIAN_POINT ( 'NONE',  ( -9.563806973793814947, 19.74097577964120376, 11.49999999999999645 ) ) ;
#66943=CARTESIAN_POINT ( 'NONE',  ( -37.61807812461461964, -23.48786465467240703, 11.44779295918255180 ) ) ;
#66944=CARTESIAN_POINT ( 'NONE',  ( -12.86601690267178100, 18.50254183665605012, -1.500000000000002220 ) ) ;
#66945=CARTESIAN_POINT ( 'NONE',  ( 17.97375762979478253, -10.76934015532128797, 11.49999999999998934 ) ) ;
#66947=CARTESIAN_POINT ( 'NONE',  ( -91.62287095715004170, -23.48783264082478794, -1.443836473390063713 ) ) ;
#66948=AXIS2_PLACEMENT_3D ( 'NONE', #16178, #85189, #55263 ) ;
#66950=ORIENTED_EDGE ( 'NONE', *, *, #79038, .F. ) ;
#66955=B_SPLINE_CURVE_WITH_KNOTS ( 'NONE', 3,
 ( #87023, #86022, #16498, #47470, #32231, #17007, #23607, #25114 ),
 .UNSPECIFIED., .F., .F.,
 ( 4, 2, 2, 4 ),
 ( -0.001224554619866347364, -0.0002241820295893631482, 0.0007761905606876210676, 0.002776935741241580609 ),
 .UNSPECIFIED. ) ;
#66956=ADVANCED_FACE ( 'NONE', ( #4260 ), #35209, .F. ) ;
#66957=CARTESIAN_POINT ( 'NONE',  ( 18.57079561221590325, -10.74342183689097574, -1.500000000000002220 ) ) ;
#66959=DIRECTION ( 'NONE',  ( 3.773278334444166432E-23, -1.000000000000000000, 0.000000000000000000 ) ) ;
#66961=CARTESIAN_POINT ( 'NONE',  ( -6.733481718715807141, 19.98004043397084928, 11.49999999999998934 ) ) ;
#66962=CARTESIAN_POINT ( 'NONE',  ( -99.56332528172060847, -25.25520022910753326, 3.790695193615264635 ) ) ;
#66968=CARTESIAN_POINT ( 'NONE',  ( 0.6065052782250800467, 22.08157775750015617, -1.500000000000002220 ) ) ;
#66970=CARTESIAN_POINT ( 'NONE',  ( -103.5228709571501042, -23.48783264082477018, -1.443836473390087916 ) ) ;
#66971=CARTESIAN_POINT ( 'NONE',  ( -70.62287095715005592, -29.50249982740957577, 7.747779886224967605 ) ) ;
#66972=CARTESIAN_POINT ( 'NONE',  ( -41.86646858058957577, -25.27955811415035470, 4.347424021778468095 ) ) ;
#66973=ADVANCED_FACE ( 'NONE', ( #11858 ), #87996, .F. ) ;
#66975=CARTESIAN_POINT ( 'NONE',  ( -100.5511821681996878, -24.40034930558991633, 0.3402023900116076804 ) ) ;
#66976=CARTESIAN_POINT ( 'NONE',  ( -2.795030477444873540, 19.22867370847827573, 11.49999999999998934 ) ) ;
#66978=CARTESIAN_POINT ( 'NONE',  ( 9.194277187580093269, -19.27880637823015419, -1.500000000000002220 ) ) ;
#66980=CARTESIAN_POINT ( 'NONE',  ( -89.80423082004377022, -25.26266127311082954, 3.981777872396911278 ) ) ;
#66981=CARTESIAN_POINT ( 'NONE',  ( -70.52287095715007581, -24.99156044556120548, 7.747789690856173195 ) ) ;
#66983=CARTESIAN_POINT ( 'NONE',  ( 21.71957326813621592, -6.446789169762093152, -1.500000000000002220 ) ) ;
#66984=B_SPLINE_SURFACE_WITH_KNOTS ( 'NONE', 3, 1, ( 
 ( #51653, #58761 ),
 ( #82593, #5468 ),
 ( #42057, #96324 ),
 ( #26813, #88717 ),
 ( #19188, #50160 ),
 ( #81097, #22671 ),
 ( #350, #30804 ),
 ( #22173, #31298 ),
 ( #21183, #92193 ),
 ( #83581, #53657 ),
 ( #46531, #13567 ),
 ( #29801, #7958 ),
 ( #85084, #6471 ),
 ( #29301, #62265 ),
 ( #44537, #60274 ),
 ( #68866, #67878 ),
 ( #52148, #99786 ),
 ( #83074, #60768 ),
 ( #37425, #75462 ) ),
 .UNSPECIFIED., .F., .F., .F.,
 ( 4, 1, 1, 1, 1, 1, 1, 1, 1, 1, 1, 1, 1, 1, 1, 1, 4 ),
 ( 2, 2 ),
 ( 0.000000000000000000, 0.06076009704672557382, 0.1197352241628591996, 0.1777568621302152985, 0.2359989679007910846, 0.2940703618108028161, 0.3537332155261553868, 0.4159726195849062780, 0.4801398374083836740, 0.5450760546750318403, 0.6087348974468034246, 0.6721778698820234377, 0.7354527509796394691, 0.7991115937514117196, 0.8642836660180990282, 0.9308370508155386913, 1.000000000000000000 ),
 ( 0.000000000000000000, 1.000000000000000000 ),
 .UNSPECIFIED. ) ;
#66987=CARTESIAN_POINT ( 'NONE',  ( -79.58492028048088684, -24.51314013834315375, 0.6176544820404122893 ) ) ;
#66988=CARTESIAN_POINT ( 'NONE',  ( 14.33573519231038063, 13.56928687979844561, 11.49999999999999645 ) ) ;
#66989=PLANE ( 'NONE',  #21290 ) ;
#66990=CARTESIAN_POINT ( 'NONE',  ( -104.6228709571500559, -29.50248528299804818, 1.056150453629042030 ) ) ;
#66992=ORIENTED_EDGE ( 'NONE', *, *, #23866, .T. ) ;
#66993=CARTESIAN_POINT ( 'NONE',  ( -59.52287095715006870, -24.50216790748205042, 0.6166512839542541702 ) ) ;
#66994=CARTESIAN_POINT ( 'NONE',  ( -29.61081252053125112, -25.26026626986611134, 3.196430263304397279 ) ) ;
#66996=CARTESIAN_POINT ( 'NONE',  ( -100.4799102492508780, -25.17353343721469372, 7.101073737836308908 ) ) ;
#66997=CARTESIAN_POINT ( 'NONE',  ( -17.57154585214776077, 12.61476001598989782, -1.500000000000002220 ) ) ;
#66998=CARTESIAN_POINT ( 'NONE',  ( -49.11088876609831289, -25.10935348367436504, 3.850712044224722685 ) ) ;
#66999=CARTESIAN_POINT ( 'NONE',  ( -14.46832242630667942, -12.86894606327920876, -1.500000000000002220 ) ) ;
#67001=CARTESIAN_POINT ( 'NONE',  ( -48.62287095715004881, -29.50250786944525672, 11.44777988621624054 ) ) ;
#67002=CARTESIAN_POINT ( 'NONE',  ( 14.04693994163893578, -13.95676237773968609, -1.500000000000002220 ) ) ;
#67003=EDGE_LOOP ( 'NONE', ( #61028, #19801, #38800, #58590 ) ) ;
#67005=CARTESIAN_POINT ( 'NONE',  ( 17.32893120472914816, 10.46255702124672027, 11.49999999999999645 ) ) ;
#67006=DIRECTION ( 'NONE',  ( 0.000000000000000000, 0.9999999999976377785, 2.173523156925979128E-06 ) ) ;
#67007=EDGE_CURVE ( 'NONE', #85588, #58867, #22295, .T. ) ;
#67009=EDGE_CURVE ( 'NONE', #67625, #48223, #20460, .T. ) ;
#67010=ORIENTED_EDGE ( 'NONE', *, *, #30893, .T. ) ;
#67016=CARTESIAN_POINT ( 'NONE',  ( -11.36185547594953249, 16.55520930037988592, 11.49999999999998934 ) ) ;
#67019=ORIENTED_EDGE ( 'NONE', *, *, #52540, .T. ) ;
#67023=CARTESIAN_POINT ( 'NONE',  ( -50.05252738782304789, -25.26258873067627775, 4.679464405298413787 ) ) ;
#67025=CARTESIAN_POINT ( 'NONE',  ( -53.62287095715005592, -23.47593901973091235, -1.443836447539009749 ) ) ;
#67026=CARTESIAN_POINT ( 'NONE',  ( -43.58953762381672448, -24.64965694238406613, 8.947790433994661896 ) ) ;
#67028=CARTESIAN_POINT ( 'NONE',  ( -118.6228709571500559, -24.51387760970725083, 9.387446482453411178 ) ) ;
#67030=CARTESIAN_POINT ( 'NONE',  ( -17.72129891523481149, -13.73837202384828515, 11.49999999999999645 ) ) ;
#67031=CARTESIAN_POINT ( 'NONE',  ( -93.62287095715005592, -24.64898659630367916, 1.056161002820827921 ) ) ;
#67032=VERTEX_POINT ( 'NONE', #89986 ) ;
#67033=CARTESIAN_POINT ( 'NONE',  ( -7.038884989605349141, -19.10714869031923513, 11.49999999999998934 ) ) ;
#67034=VECTOR ( 'NONE', #33372, 1000.000000000000114 ) ;
#67035=ORIENTED_EDGE ( 'NONE', *, *, #97795, .T. ) ;
#67036=CARTESIAN_POINT ( 'NONE',  ( -8.204236019480731557, -21.45505762417899831, -1.500000000000002220 ) ) ;
#67037=CARTESIAN_POINT ( 'NONE',  ( -89.62287095715004170, -23.47593901973091235, -1.443836447539002865 ) ) ;
#67038=EDGE_LOOP ( 'NONE', ( #73078, #51064, #8025, #57844 ) ) ;
#67040=CARTESIAN_POINT ( 'NONE',  ( -77.52212609141741950, -23.48786465467240703, 11.44779295918254647 ) ) ;
#67041=CARTESIAN_POINT ( 'NONE',  ( -77.52287095715007581, -23.48783264082476308, -1.443836473390091912 ) ) ;
#67042=CARTESIAN_POINT ( 'NONE',  ( 21.18767802922067034, -0.7184367399587067160, 11.49999999999999645 ) ) ;
#67045=CARTESIAN_POINT ( 'NONE',  ( 7.527104757430762128, -20.84474501729809859, 11.49999999999998934 ) ) ;
#67046=CARTESIAN_POINT ( 'NONE',  ( 14.24201292913401140, 14.87178044790754328, -1.500000000000002220 ) ) ;
#67047=EDGE_LOOP ( 'NONE', ( #3130, #5532, #92715, #34258 ) ) ;
#67048=VERTEX_POINT ( 'NONE', #14340 ) ;
#67050=CARTESIAN_POINT ( 'NONE',  ( -49.62287095715004881, -24.33832256526968862, 0.1851278514119874263 ) ) ;
#67055=CARTESIAN_POINT ( 'NONE',  ( -108.5228709571500616, -24.65952944569304961, 1.056160979905704123 ) ) ;
#67057=CARTESIAN_POINT ( 'NONE',  ( -15.22196369898608737, 14.14466773073655581, -1.500000000000002220 ) ) ;
#67058=CARTESIAN_POINT ( 'NONE',  ( 14.05712878599199200, -16.60762996970646199, 11.49999999999999645 ) ) ;
#67061=CARTESIAN_POINT ( 'NONE',  ( -100.6903391770916016, -25.18886833083715970, 3.321861835454170464 ) ) ;
#67062=CARTESIAN_POINT ( 'NONE',  ( -34.62287095715007013, -23.47596703998600276, 11.44779298504227505 ) ) ;
#67063=CARTESIAN_POINT ( 'NONE',  ( -115.5895851036066944, -24.52300882791528736, 0.6510814631126266017 ) ) ;
#67064=CARTESIAN_POINT ( 'NONE',  ( 6.649717926671450563, 21.43536518531312396, -1.500000000000002220 ) ) ;
#67066=CARTESIAN_POINT ( 'NONE',  ( -65.55177604255820256, -24.15503026093916361, -0.2815557561904382111 ) ) ;
#67067=ORIENTED_EDGE ( 'NONE', *, *, #41680, .T. ) ;
#67068=CARTESIAN_POINT ( 'NONE',  ( -71.60141483542169283, -25.30054065008881636, 5.617309697255326029 ) ) ;
#67069=CARTESIAN_POINT ( 'NONE',  ( -119.4728709571500502, -25.21113200442379565, 5.000950862978366551 ) ) ;
#67071=EDGE_LOOP ( 'NONE', ( #31839, #37246, #88128, #51780 ) ) ;
#67075=EDGE_CURVE ( 'NONE', #53340, #63553, #98583, .T. ) ;
#67076=CARTESIAN_POINT ( 'NONE',  ( 21.27783752795556538, -0.9766432368044721812, -1.500000000000002220 ) ) ;
#67079=CARTESIAN_POINT ( 'NONE',  ( 12.58402814888991372, -17.87355554032721372, 11.49999999999998934 ) ) ;
#67080=DIRECTION ( 'NONE',  ( 0.000000000000000000, -2.173523156925980399E-06, 0.9999999999976378895 ) ) ;
#67081=CARTESIAN_POINT ( 'NONE',  ( 22.47986593085892437, -3.190245585651162230, 11.49999999999998934 ) ) ;
#67082=CARTESIAN_POINT ( 'NONE',  ( -87.62287095715004170, -29.50250786944525672, 11.44777988621623344 ) ) ;
#67084=CARTESIAN_POINT ( 'NONE',  ( 16.22650188657148362, -14.79325693486936188, -1.500000000000002220 ) ) ;
#67085=CARTESIAN_POINT ( 'NONE',  ( -39.52287095715008292, -23.48783264082476308, -1.443836473390098574 ) ) ;
#67086=VERTEX_POINT ( 'NONE', #52428 ) ;
#67088=DIRECTION ( 'NONE',  ( -3.773278334453079030E-23, 0.9999999999976377785, 2.173523156925979128E-06 ) ) ;
#67089=B_SPLINE_CURVE_WITH_KNOTS ( 'NONE', 3,
 ( #29928, #76094, #54287, #69500, #39547, #78087 ),
 .UNSPECIFIED., .F., .F.,
 ( 4, 2, 4 ),
 ( 0.000000000000000000, 0.001380764517854760629, 0.002761529035709521258 ),
 .UNSPECIFIED. ) ;
#67090=EDGE_CURVE ( 'NONE', #37715, #55534, #29077, .T. ) ;
#67091=EDGE_CURVE ( 'NONE', #75143, #77563, #93844, .T. ) ;
#67092=ORIENTED_EDGE ( 'NONE', *, *, #54912, .F. ) ;
#67094=CARTESIAN_POINT ( 'NONE',  ( -84.64454908083816065, -23.48786465467241413, 11.44779295918254469 ) ) ;
#67095=CARTESIAN_POINT ( 'NONE',  ( -39.58953762381672448, -23.48783264082477373, -1.443836473390072594 ) ) ;
#67096=EDGE_CURVE ( 'NONE', #92960, #64351, #63499, .T. ) ;
#67097=FACE_BOUND ( 'NONE', #38136, .T. ) ;
#67098=CARTESIAN_POINT ( 'NONE',  ( -16.85803360905838488, 12.98640638483674259, 11.49999999999998934 ) ) ;
#67099=CARTESIAN_POINT ( 'NONE',  ( -98.50937779290613605, -24.51419770103155926, 9.386484678747176957 ) ) ;
#67101=CARTESIAN_POINT ( 'NONE',  ( -85.63005396505535316, -24.63355581998386157, 0.9682620441943895484 ) ) ;
#67102=CARTESIAN_POINT ( 'NONE',  ( -33.65005778919723411, -23.96119346886880308, -0.6495511937832006977 ) ) ;
#67103=CARTESIAN_POINT ( 'NONE',  ( -90.52287095715006160, -24.99132157543165889, 2.256160258750667502 ) ) ;
#67105=CARTESIAN_POINT ( 'NONE',  ( -10.82925958622295859, 16.30987832687952022, 11.49999999999999645 ) ) ;
#67106=CARTESIAN_POINT ( 'NONE',  ( -66.62287095715002749, -23.96177878511307568, 10.65340807706330217 ) ) ;
#67108=EDGE_CURVE ( 'NONE', #38334, #20641, #6677, .T. ) ;
#67110=CARTESIAN_POINT ( 'NONE',  ( -97.52287095715001897, -24.34917612406837861, 0.1852690917426576545 ) ) ;
#67111=CARTESIAN_POINT ( 'NONE',  ( -99.33961253015885973, -25.31506754800236791, 5.119446277803796796 ) ) ;
#67113=CARTESIAN_POINT ( 'NONE',  ( -40.62287095715003460, -24.51254535404254398, 9.355368623467652966 ) ) ;
#67114=CARTESIAN_POINT ( 'NONE',  ( -18.83419513347712737, -5.836681878196540829, -1.500000000000002220 ) ) ;
#67115=ADVANCED_FACE ( 'NONE', ( #97593 ), #61545, .F. ) ;
#67116=VERTEX_POINT ( 'NONE', #92464 ) ;
#67117=DIRECTION ( 'NONE',  ( 0.000000000000000000, -2.173523156925979975E-06, 0.9999999999976378895 ) ) ;
#67118=CARTESIAN_POINT ( 'NONE',  ( -57.52287095715005449, -23.47596703998600631, 11.44779298504228926 ) ) ;
#67119=ADVANCED_FACE ( 'NONE', ( #93969 ), #24462, .T. ) ;
#67121=ORIENTED_EDGE ( 'NONE', *, *, #29868, .T. ) ;
#67122=CARTESIAN_POINT ( 'NONE',  ( -103.5228709571500758, -29.50250243563736774, 8.947779886222138046 ) ) ;
#67123=CARTESIAN_POINT ( 'NONE',  ( -84.52287095715007581, -23.48783264082477018, -1.443836473390090802 ) ) ;
#67124=CARTESIAN_POINT ( 'NONE',  ( -69.62287095715004170, -23.72747288104441665, -1.053458166803662444 ) ) ;
#67125=CARTESIAN_POINT ( 'NONE',  ( -84.52287095715006160, -29.50248528299804818, 1.056150453629038477 ) ) ;
#67127=CARTESIAN_POINT ( 'NONE',  ( -70.35895856474228083, -25.24515042133736031, 5.313173755051356473 ) ) ;
#67128=CARTESIAN_POINT ( 'NONE',  ( -91.52287095715000476, -24.33927499327855060, 9.819080762295806508 ) ) ;
#67129=CARTESIAN_POINT ( 'NONE',  ( 19.20567810191101898, 5.375360269454119155, 11.49999999999998934 ) ) ;
#67130=B_SPLINE_CURVE_WITH_KNOTS ( 'NONE', 3,
 ( #85927, #39742, #70700, #76786, #1195, #7289 ),
 .UNSPECIFIED., .F., .F.,
 ( 4, 2, 4 ),
 ( 0.000000000000000000, 0.001380901958385383774, 0.002761803916770767548 ),
 .UNSPECIFIED. ) ;
#67132=CARTESIAN_POINT ( 'NONE',  ( -71.55620429048337883, -23.47593901973091235, -1.443836447539006196 ) ) ;
#67133=CARTESIAN_POINT ( 'NONE',  ( -0.0004653795375827224552, -23.04397529616130313, 5.579469812630287073 ) ) ;
#67134=VERTEX_POINT ( 'NONE', #8746 ) ;
#67139=CARTESIAN_POINT ( 'NONE',  ( -119.5920062970955087, -23.73766607897670511, -1.055555164236450238 ) ) ;
#67140=CARTESIAN_POINT ( 'NONE',  ( -80.60939578119689486, -23.48786465467241413, 11.44779295918254824 ) ) ;
#67141=CARTESIAN_POINT ( 'NONE',  ( -49.74369414166533687, -25.31543073408252909, 4.940877929217667663 ) ) ;
#67142=CARTESIAN_POINT ( 'NONE',  ( -81.51309679017218457, -23.96119346886881019, -0.6495511937831893734 ) ) ;
#67143=EDGE_CURVE ( 'NONE', #79632, #36107, #39684, .T. ) ;
#67145=B_SPLINE_CURVE_WITH_KNOTS ( 'NONE', 3,
 ( #21117, #44980, #37854, #75905 ),
 .UNSPECIFIED., .F., .F.,
 ( 4, 4 ),
 ( 0.6492381622116810691, 0.6502389092524463177 ),
 .UNSPECIFIED. ) ;
#67147=ORIENTED_EDGE ( 'NONE', *, *, #8547, .F. ) ;
#67150=ORIENTED_EDGE ( 'NONE', *, *, #21732, .T. ) ;
#67151=CARTESIAN_POINT ( 'NONE',  ( -11.13811422090317294, 16.88724661786912762, -1.500000000000002220 ) ) ;
#67152=CARTESIAN_POINT ( 'NONE',  ( -69.45360722279276899, -25.31510505358946261, 5.121476220657646294 ) ) ;
#67153=FACE_OUTER_BOUND ( 'NONE', #90106, .T. ) ;
#67155=ORIENTED_EDGE ( 'NONE', *, *, #21262, .F. ) ;
#67156=CARTESIAN_POINT ( 'NONE',  ( -79.10627061423527095, -25.31353510145896024, 5.240107987869434325 ) ) ;
#67157=DIRECTION ( 'NONE',  ( -3.773278334453079618E-23, 0.9999999999976377785, 2.173523156925979975E-06 ) ) ;
#67158=CARTESIAN_POINT ( 'NONE',  ( 12.62869658624171976, -15.57725692549414376, -1.500000000000002220 ) ) ;
#67159=CARTESIAN_POINT ( 'NONE',  ( 19.96068868648078620, -6.529529906025321573, 11.49999999999999645 ) ) ;
#67161=CARTESIAN_POINT ( 'NONE',  ( -70.63765949830232671, -24.40133493613049964, 9.663955038902802386 ) ) ;
#67162=CARTESIAN_POINT ( 'NONE',  ( 11.82310115920509830, 18.66461490495635545, -1.500000000000002220 ) ) ;
#67164=DIRECTION ( 'NONE',  ( -1.000000000000000000, -3.773278334444166432E-23, -8.201307841325785021E-29 ) ) ;
#67165=CARTESIAN_POINT ( 'NONE',  ( -50.02027282914984596, -25.27344770931672358, 3.346181230627190306 ) ) ;
#67167=CARTESIAN_POINT ( 'NONE',  ( -99.80308396037207785, -25.14437514330485257, 2.967792536799680470 ) ) ;
#67168=B_SPLINE_SURFACE_WITH_KNOTS ( 'NONE', 3, 1, ( 
 ( #65331, #3418 ),
 ( #27735, #33846 ),
 ( #26236, #19610 ),
 ( #33337, #73907 ),
 ( #35356, #89137 ),
 ( #12003, #64834 ),
 ( #96743, #2916 ),
 ( #72423, #50573 ),
 ( #25733, #95745 ),
 ( #57209, #88142 ),
 ( #18611, #4405 ),
 ( #3913, #66317 ),
 ( #20113, #49585 ),
 ( #42481, #80519 ),
 ( #10006, #26735 ),
 ( #11011, #40964 ),
 ( #41978, #71924 ),
 ( #72920, #2408 ),
 ( #96251, #57697 ),
 ( #88642, #19112 ),
 ( #50084, #81024 ),
 ( #64329, #95246 ),
 ( #56707, #87639 ) ),
 .UNSPECIFIED., .F., .F., .F.,
 ( 4, 1, 1, 1, 1, 1, 1, 1, 1, 1, 1, 1, 1, 1, 1, 1, 1, 1, 1, 1, 4 ),
 ( 2, 2 ),
 ( 0.000000000000000000, 0.06038661931106217851, 0.1208832485859971800, 0.1827546186251399196, 0.2478110297583515365, 0.2812991000432492061, 0.3150876241506573860, 0.3497023955502753800, 0.3848565811185556962, 0.4209661972261026786, 0.4585111882611394019, 0.4971747221273126738, 0.5376020478662696389, 0.5805030184200120624, 0.6274675400267047953, 0.6783882095592436157, 0.7339832205925607145, 0.7937467045508352914, 0.8577136721607322434, 0.9266978643613863476, 1.000000000000000000 ),
 ( 0.000000000000000000, 1.000000000000000000 ),
 .UNSPECIFIED. ) ;
#67170=ORIENTED_EDGE ( 'NONE', *, *, #7791, .F. ) ;
#67172=CARTESIAN_POINT ( 'NONE',  ( -55.52287095715009002, -24.63287334234179582, 0.9662140553045320823 ) ) ;
#67173=CARTESIAN_POINT ( 'NONE',  ( -44.52287095715006160, -29.50250243563736774, 8.947779886222148704 ) ) ;
#67174=CARTESIAN_POINT ( 'NONE',  ( -89.62287095715002749, -23.48783264082478439, -1.443836473390063713 ) ) ;
#67175=CARTESIAN_POINT ( 'NONE',  ( 10.47388184937329214, 17.72644800832989986, -1.500000000000002220 ) ) ;
#67176=CARTESIAN_POINT ( 'NONE',  ( 5.689979955356517571, -20.79666814084963278, 11.49999999999999645 ) ) ;
#67177=ORIENTED_EDGE ( 'NONE', *, *, #40260, .T. ) ;
#67178=CARTESIAN_POINT ( 'NONE',  ( -91.62826352414620601, -24.34968618360934656, 0.1864209137778843617 ) ) ;
#67179=CARTESIAN_POINT ( 'NONE',  ( -53.62287095715005592, -23.47596703998600276, 11.44779298504227683 ) ) ;
#67180=CARTESIAN_POINT ( 'NONE',  ( -129.6228709571500133, -23.96127896941632685, -0.6493128931037762674 ) ) ;
#67181=CARTESIAN_POINT ( 'NONE',  ( 10.24050353823403192, -19.87907451059620456, 11.49999999999998934 ) ) ;
#67182=CARTESIAN_POINT ( 'NONE',  ( -34.52287095715005449, -23.73934037231755312, 11.05740245334329153 ) ) ;
#67183=CARTESIAN_POINT ( 'NONE',  ( -84.59526730009702078, -23.96119346886880663, -0.6495511937832096905 ) ) ;
#67184=VERTEX_POINT ( 'NONE', #1135 ) ;
#67185=DIRECTION ( 'NONE',  ( -3.773278334453079030E-23, 0.9999999999976377785, 2.173523156925979128E-06 ) ) ;
#67187=CARTESIAN_POINT ( 'NONE',  ( 14.99592430652175956, 14.54719766626331889, -1.500000000000002220 ) ) ;
#67188=ORIENTED_EDGE ( 'NONE', *, *, #3748, .F. ) ;
#67192=ORIENTED_EDGE ( 'NONE', *, *, #85544, .F. ) ;
#67193=CARTESIAN_POINT ( 'NONE',  ( -100.5869784172404877, -24.73531770709095312, 8.716586749053508498 ) ) ;
#67194=CARTESIAN_POINT ( 'NONE',  ( -21.09505027744838657, -1.104435277493458045, -1.500000000000002220 ) ) ;
#67195=ORIENTED_EDGE ( 'NONE', *, *, #42780, .T. ) ;
#67196=CARTESIAN_POINT ( 'NONE',  ( -94.52287095715003318, -24.66019654487199730, 8.947790411086124607 ) ) ;
#67197=CARTESIAN_POINT ( 'NONE',  ( -102.6228709571500701, -24.50321055353805377, 9.387540953477524042 ) ) ;
#67200=EDGE_CURVE ( 'NONE', #39942, #77983, #81627, .T. ) ;
#67201=CARTESIAN_POINT ( 'NONE',  ( -76.50396469980680081, -24.35071581493543036, 9.817618358456028815 ) ) ;
#67203=CARTESIAN_POINT ( 'NONE',  ( 17.47290450027814757, -12.96279059203284767, -1.500000000000002220 ) ) ;
#67205=CARTESIAN_POINT ( 'NONE',  ( 13.76814385225720372, 17.53657229028232223, 11.49999999999999645 ) ) ;
#67206=EDGE_LOOP ( 'NONE', ( #80899, #33832, #48573, #92144 ) ) ;
#67207=FACE_OUTER_BOUND ( 'NONE', #9727, .T. ) ;
#67209=CARTESIAN_POINT ( 'NONE',  ( -101.5228709571500758, -23.47593901973090524, -1.443836447538996426 ) ) ;
#67213=EDGE_CURVE ( 'NONE', #39944, #16912, #69648, .T. ) ;
#67218=CARTESIAN_POINT ( 'NONE',  ( -52.58953762381672448, -23.48786465467240703, 11.44779295918255002 ) ) ;
#67219=CARTESIAN_POINT ( 'NONE',  ( -67.62287095715005592, -23.48786465467241058, 11.44779295918254647 ) ) ;
#67220=CARTESIAN_POINT ( 'NONE',  ( -16.24122463664219396, 10.56255597858309869, 11.49999999999998934 ) ) ;
#67223=EDGE_LOOP ( 'NONE', ( #19836, #32330, #34987, #36593 ) ) ;
#67224=CARTESIAN_POINT ( 'NONE',  ( -12.28997142660015740, 14.97987746540053422, 11.49999999999999645 ) ) ;
#67225=CARTESIAN_POINT ( 'NONE',  ( -47.62287095715006302, -23.47596703998600276, 11.44779298504227505 ) ) ;
#67227=FACE_OUTER_BOUND ( 'NONE', #27703, .T. ) ;
#67229=CARTESIAN_POINT ( 'NONE',  ( -65.52287095715006160, -23.47596703998600631, 11.44779298504228748 ) ) ;
#67230=CARTESIAN_POINT ( 'NONE',  ( -36.52287095715006870, -24.35013146730203815, 9.818937971375104823 ) ) ;
#67231=CARTESIAN_POINT ( 'NONE',  ( 16.12930680145378304, -11.13525102954884893, 11.49999999999998934 ) ) ;
#67232=CARTESIAN_POINT ( 'NONE',  ( -46.58180868254443396, -24.51314013834315020, 0.6176544820404077374 ) ) ;
#67235=CARTESIAN_POINT ( 'NONE',  ( -16.67190562677319932, -13.68652177170558204, -1.500000000000002220 ) ) ;
#67236=CARTESIAN_POINT ( 'NONE',  ( -33.62373659705630757, -24.66019654487198665, 8.947790411086133489 ) ) ;
#67237=CARTESIAN_POINT ( 'NONE',  ( -70.78633892220865675, -25.12219122934108384, 7.001279615086478003 ) ) ;
#67238=DIRECTION ( 'NONE',  ( -3.773278334453079030E-23, 0.9999999999976377785, 2.173523156925979128E-06 ) ) ;
#67240=CARTESIAN_POINT ( 'NONE',  ( -0.3492834940180428727, 22.98956000712751546, -1.500000000000002220 ) ) ;
#67242=CARTESIAN_POINT ( 'NONE',  ( -49.57749393427013729, -24.65952944569304606, 1.056160979905696129 ) ) ;
#67243=CARTESIAN_POINT ( 'NONE',  ( -8.513533612778267923, 18.29693335657625042, 11.49999999999999645 ) ) ;
#67244=CARTESIAN_POINT ( 'NONE',  ( -109.3293036055952143, -25.10927482606251715, 3.229615370203269720 ) ) ;
#67245=DIRECTION ( 'NONE',  ( -3.773278334453079030E-23, 0.9999999999976377785, 2.173523156925979128E-06 ) ) ;
#67246=LINE ( 'NONE', #44905, #13366 ) ;
#67248=CARTESIAN_POINT ( 'NONE',  ( -111.2332490450528582, -25.18425693141708521, 3.802242211139469141 ) ) ;
#67249=CARTESIAN_POINT ( 'NONE',  ( -14.63867168220055781, -13.42826565525684579, -1.500000000000002220 ) ) ;
#67251=CARTESIAN_POINT ( 'NONE',  ( -19.69265041987409859, 1.759638296948408787, -1.500000000000002220 ) ) ;
#67256=CARTESIAN_POINT ( 'NONE',  ( 20.67342648114324533, -1.018679444107209342, 11.49999999999999645 ) ) ;
#67257=DIRECTION ( 'NONE',  ( -3.773278334453079618E-23, 0.9999999999976377785, 2.173523156925979975E-06 ) ) ;
#67258=EDGE_CURVE ( 'NONE', #70398, #66681, #61156, .T. ) ;
#67261=B_SPLINE_CURVE_WITH_KNOTS ( 'NONE', 3,
 ( #52322, #5636, #98975, #83257, #73657, #12237 ),
 .UNSPECIFIED., .F., .F.,
 ( 4, 2, 4 ),
 ( 1.570887131794638196E-05, 0.001396322306279762591, 0.002776935741241578874 ),
 .UNSPECIFIED. ) ;
#67262=CARTESIAN_POINT ( 'NONE',  ( -44.62287095715004881, -23.47596703998600631, 11.44779298504227505 ) ) ;
#67263=CARTESIAN_POINT ( 'NONE',  ( 20.10346781357453949, 10.43426432342431553, 11.49999999999999645 ) ) ;
#67264=VERTEX_POINT ( 'NONE', #16345 ) ;
#67267=FACE_OUTER_BOUND ( 'NONE', #56291, .T. ) ;
#67270=ORIENTED_EDGE ( 'NONE', *, *, #82922, .F. ) ;
#67272=ORIENTED_EDGE ( 'NONE', *, *, #45630, .T. ) ;
#67274=CARTESIAN_POINT ( 'NONE',  ( 22.85402955525884394, -0.1436109537974766814, 11.49999999999998934 ) ) ;
#67275=CARTESIAN_POINT ( 'NONE',  ( -29.52199330670222110, -23.40092668919113450, -1.443836171194816886 ) ) ;
#67276=CARTESIAN_POINT ( 'NONE',  ( -11.65619939812097527, 18.16556634249905855, -1.500000000000002220 ) ) ;
#67278=CARTESIAN_POINT ( 'NONE',  ( -65.52287095715006160, -25.00158670708909625, 2.256160236439166411 ) ) ;
#67279=CARTESIAN_POINT ( 'NONE',  ( -20.59131556071872282, -9.131246169528550283, 11.49999999999999645 ) ) ;
#67280=ORIENTED_EDGE ( 'NONE', *, *, #32717, .F. ) ;
#67281=CARTESIAN_POINT ( 'NONE',  ( -70.27422298781921484, -25.24754245836512467, 4.851635288312657224 ) ) ;
#67282=CARTESIAN_POINT ( 'NONE',  ( 17.26801960494244881, -13.64313956103151071, -1.500000000000002220 ) ) ;
#67283=CARTESIAN_POINT ( 'NONE',  ( -64.52287095715009002, -23.72747288104470087, -1.053458166803226126 ) ) ;
#67284=CARTESIAN_POINT ( 'NONE',  ( -27.75582626765746497, -25.21724993721676711, 7.602200292291605876 ) ) ;
#67285=ORIENTED_EDGE ( 'NONE', *, *, #81631, .F. ) ;
#67287=CARTESIAN_POINT ( 'NONE',  ( -90.51647507451308172, -23.85049219812686871, 10.88485053497527844 ) ) ;
#67288=ORIENTED_EDGE ( 'NONE', *, *, #24438, .T. ) ;
#67289=CARTESIAN_POINT ( 'NONE',  ( -108.6228709571500559, -23.47593901973091235, -1.443836447538999312 ) ) ;
#67292=CARTESIAN_POINT ( 'NONE',  ( -65.52287095715006160, -23.84047902841601640, -0.8780736468305708753 ) ) ;
#67294=CARTESIAN_POINT ( 'NONE',  ( -57.57870244156648454, -24.65952944569304606, 1.056160979905698571 ) ) ;
#67295=CARTESIAN_POINT ( 'NONE',  ( 19.51578053514377586, 5.923290232019536639, -1.500000000000002220 ) ) ;
#67298=CARTESIAN_POINT ( 'NONE',  ( -92.52287095715011844, -23.96177878511310055, 10.65340807706329507 ) ) ;
#67300=CARTESIAN_POINT ( 'NONE',  ( -44.62287095715004881, -29.50248528299804818, 1.056150453629031594 ) ) ;
#67302=DIRECTION ( 'NONE',  ( 3.773278334444167608E-23, -1.000000000000000000, 0.000000000000000000 ) ) ;
#67303=CARTESIAN_POINT ( 'NONE',  ( -28.27652290204276042, -25.26248058196737745, 8.166124215670606645 ) ) ;
#67305=CARTESIAN_POINT ( 'NONE',  ( 5.171613189315443115, 20.13430294385436881, -1.500000000000002220 ) ) ;
#67309=FACE_OUTER_BOUND ( 'NONE', #40963, .T. ) ;
#67310=CARTESIAN_POINT ( 'NONE',  ( -56.55620429048342146, -23.47596703998600276, 11.44779298504227505 ) ) ;
#67314=ADVANCED_FACE ( 'NONE', ( #87363 ), #4138, .F. ) ;
#67315=CARTESIAN_POINT ( 'NONE',  ( -64.52287095715010423, -24.51387760970724727, 9.387446482453412955 ) ) ;
#67317=CARTESIAN_POINT ( 'NONE',  ( -70.55843555340263151, -25.31201593592794907, 5.327474662351524337 ) ) ;
#67318=CARTESIAN_POINT ( 'NONE',  ( -12.03526013704878039, -18.61824004984164560, 11.49999999999999645 ) ) ;
#67319=ORIENTED_EDGE ( 'NONE', *, *, #63767, .T. ) ;
#67320=LINE ( 'NONE', #28750, #10686 ) ;
#67322=CARTESIAN_POINT ( 'NONE',  ( 21.37280783159109276, 7.349196219051140844, -1.500000000000002220 ) ) ;
#67323=ADVANCED_FACE ( 'NONE', ( #81253 ), #96003, .T. ) ;
#67324=CARTESIAN_POINT ( 'NONE',  ( -115.5550126193648737, -24.15602025860897584, 10.28564288303533836 ) ) ;
#67325=ORIENTED_EDGE ( 'NONE', *, *, #36031, .F. ) ;
#67326=ADVANCED_FACE ( 'NONE', ( #11735 ), #33583, .T. ) ;
#67329=CARTESIAN_POINT ( 'NONE',  ( -69.62287095715005592, -23.47593901973091235, -1.443836447539006196 ) ) ;
#67334=CARTESIAN_POINT ( 'NONE',  ( -126.5228709571500332, -24.51283580621365843, 0.6167428607019861397 ) ) ;
#67335=CARTESIAN_POINT ( 'NONE',  ( -21.62769966018443313, 5.350386031573528989, -1.500000000000002220 ) ) ;
#67337=FACE_OUTER_BOUND ( 'NONE', #57459, .T. ) ;
#67338=EDGE_CURVE ( 'NONE', #71801, #9237, #13855, .T. ) ;
#67340=EDGE_LOOP ( 'NONE', ( #18247, #60835, #64356, #69748 ) ) ;
#67343=CARTESIAN_POINT ( 'NONE',  ( -103.6228709571500559, -29.50248528299804818, 1.056150453629042030 ) ) ;
#67344=AXIS2_PLACEMENT_3D ( 'NONE', #56439, #95480, #25463 ) ;
#67345=LINE ( 'NONE', #53990, #98171 ) ;
#67347=CARTESIAN_POINT ( 'NONE',  ( -19.51626497420292239, -0.3564122556526727048, 11.49999999999998934 ) ) ;
#67348=CARTESIAN_POINT ( 'NONE',  ( -20.95461191387366284, 4.708766595171775649, 11.49999999999998934 ) ) ;
#67349=B_SPLINE_CURVE_WITH_KNOTS ( 'NONE', 3,
 ( #89484, #89983, #19465, #20456, #74747, #51429 ),
 .UNSPECIFIED., .F., .F.,
 ( 4, 2, 4 ),
 ( 0.000000000000000000, 0.001380764517854761496, 0.002761529035709522992 ),
 .UNSPECIFIED. ) ;
#67352=CARTESIAN_POINT ( 'NONE',  ( -126.6228709571500559, -29.50248528299804818, 1.056150453629047137 ) ) ;
#67353=CARTESIAN_POINT ( 'NONE',  ( 18.64237364862239943, 13.12531859369229359, -1.500000000000002220 ) ) ;
#67355=CARTESIAN_POINT ( 'NONE',  ( -39.52287095715006870, -24.64898659630528144, 1.056161002820819261 ) ) ;
#67356=CARTESIAN_POINT ( 'NONE',  ( -29.24636659181000198, -29.50249372523856195, 4.940277699495910113 ) ) ;
#67357=CARTESIAN_POINT ( 'NONE',  ( 10.17626895549074817, -17.22257424524772418, 11.49999999999999645 ) ) ;
#67359=CARTESIAN_POINT ( 'NONE',  ( -43.52287095715006160, -24.65952944569304606, 1.056160979905691910 ) ) ;
#67361=ORIENTED_EDGE ( 'NONE', *, *, #50284, .F. ) ;
#67362=CARTESIAN_POINT ( 'NONE',  ( -83.52287095715001897, -24.66019654487199375, 8.947790411086122830 ) ) ;
#67363=EDGE_CURVE ( 'NONE', #46021, #42205, #17353, .T. ) ;
#67365=CARTESIAN_POINT ( 'NONE',  ( 12.24854465327799424, 17.96525243877979605, -1.500000000000002220 ) ) ;
#67366=CARTESIAN_POINT ( 'NONE',  ( -88.88918693012689687, -25.26877915520014639, 5.947789088310639904 ) ) ;
#67367=CARTESIAN_POINT ( 'NONE',  ( 18.72186718581493636, -5.619560887262019300, -1.500000000000002220 ) ) ;
#67370=ORIENTED_EDGE ( 'NONE', *, *, #27940, .T. ) ;
#67373=PLANE ( 'NONE',  #45148 ) ;
#67375=CARTESIAN_POINT ( 'NONE',  ( -19.38928925021375349, 6.733644070511561885, 11.49999999999999645 ) ) ;
#67376=CARTESIAN_POINT ( 'NONE',  ( -49.85642534923032798, -25.30192753786928606, 5.303853196035516859 ) ) ;
#67377=CARTESIAN_POINT ( 'NONE',  ( -40.52287095715005449, -23.48783264082476308, -1.443836473390097908 ) ) ;
#67383=EDGE_CURVE ( 'NONE', #48489, #64351, #43204, .T. ) ;
#67384=CARTESIAN_POINT ( 'NONE',  ( -61.62287095715002039, -24.33832256526968862, 0.1851278514119845120 ) ) ;
#67385=EDGE_LOOP ( 'NONE', ( #52602, #79527, #54403, #23674 ) ) ;
#67386=CARTESIAN_POINT ( 'NONE',  ( -109.6228709571500559, -29.50248528299804818, 1.056150453629043584 ) ) ;
#67387=CARTESIAN_POINT ( 'NONE',  ( -22.27228905017084060, 5.866681652885556986, 11.49999999999999645 ) ) ;
#67388=CARTESIAN_POINT ( 'NONE',  ( -10.92962168092244823, 19.99562239114850826, -1.500000000000002220 ) ) ;
#67390=B_SPLINE_CURVE_WITH_KNOTS ( 'NONE', 3,
 ( #45808, #29079, #60053, #76241 ),
 .UNSPECIFIED., .F., .F.,
 ( 4, 4 ),
 ( 0.000000000000000000, 1.000000000000000000 ),
 .UNSPECIFIED. ) ;
#67394=CARTESIAN_POINT ( 'NONE',  ( -99.60147378138974261, -25.30157691793918318, 4.950471116695807972 ) ) ;
#67395=CARTESIAN_POINT ( 'NONE',  ( 21.48171311866277122, -4.276277801222842179, -1.500000000000002220 ) ) ;
#67398=AXIS2_PLACEMENT_3D ( 'NONE', #61901, #8100, #484 ) ;
#67400=CARTESIAN_POINT ( 'NONE',  ( -28.62287095715006657, -24.18442083929187092, 0.1849424278035973201 ) ) ;
#67404=AXIS2_PLACEMENT_3D ( 'NONE', #49225, #57833, #18743 ) ;
#67405=CARTESIAN_POINT ( 'NONE',  ( 1.124825640313904973, 20.40429917142216354, 11.49999999999998934 ) ) ;
#67406=ORIENTED_EDGE ( 'NONE', *, *, #14244, .F. ) ;
#67407=VECTOR ( 'NONE', #58504, 1000.000000000000114 ) ;
#67408=ORIENTED_EDGE ( 'NONE', *, *, #45291, .T. ) ;
#67411=CARTESIAN_POINT ( 'NONE',  ( 15.83906049732654608, 16.74391201645830662, 11.49999999999998934 ) ) ;
#67412=CARTESIAN_POINT ( 'NONE',  ( -88.62287095715004170, -29.50250243563736774, 8.947779886222139822 ) ) ;
#67413=CARTESIAN_POINT ( 'NONE',  ( -3.766600276044322904, -19.90762401167813067, -1.500000000000002220 ) ) ;
#67415=ORIENTED_EDGE ( 'NONE', *, *, #62332, .T. ) ;
#67416=CARTESIAN_POINT ( 'NONE',  ( -29.27679109283166170, -24.91542385526720338, 7.636915180611340226 ) ) ;
#67419=CARTESIAN_POINT ( 'NONE',  ( -95.58652457540902958, -24.73486907724918282, 1.287355809206966128 ) ) ;
#67420=CARTESIAN_POINT ( 'NONE',  ( -99.54828946340249729, -24.51419770103158413, 9.386484678747176957 ) ) ;
#67421=CARTESIAN_POINT ( 'NONE',  ( 14.45597713831175035, -15.85640774750547344, 11.49999999999999645 ) ) ;
#67423=CARTESIAN_POINT ( 'NONE',  ( -77.62287095715007013, -23.48783264082478794, -1.443836473390065933 ) ) ;
#67424=ORIENTED_EDGE ( 'NONE', *, *, #280, .T. ) ;
#67425=CARTESIAN_POINT ( 'NONE',  ( -10.81534556030752725, -17.66751395530895152, 11.49999999999998934 ) ) ;
#67427=CARTESIAN_POINT ( 'NONE',  ( -28.47400090564692832, -24.49516158990158843, 1.056161677404373611 ) ) ;
#67431=CARTESIAN_POINT ( 'NONE',  ( 9.933205088616889000, -18.45388779576350302, -1.500000000000002220 ) ) ;
#67432=ADVANCED_FACE ( 'NONE', ( #97476 ), #12226, .F. ) ;
#67433=CARTESIAN_POINT ( 'NONE',  ( 1.410849576418898632, -21.91845101833037290, 11.49999999999999645 ) ) ;
#67434=CARTESIAN_POINT ( 'NONE',  ( -37.52201665554768795, -23.48786465467240347, 11.44779295918255357 ) ) ;
#67435=CARTESIAN_POINT ( 'NONE',  ( -19.74168752133572724, 10.86179948771369297, -1.500000000000002220 ) ) ;
#67436=CARTESIAN_POINT ( 'NONE',  ( -20.44905293368100985, -4.654758753755802836, -1.500000000000002220 ) ) ;
#67438=CARTESIAN_POINT ( 'NONE',  ( -119.6284939267775798, -23.48786465467241769, 11.44779295918253581 ) ) ;
#67440=ORIENTED_EDGE ( 'NONE', *, *, #83577, .T. ) ;
#67441=ADVANCED_FACE ( 'NONE', ( #60435 ), #91357, .T. ) ;
#67442=VERTEX_POINT ( 'NONE', #28960 ) ;
#67443=VERTEX_POINT ( 'NONE', #35591 ) ;
#67444=ADVANCED_FACE ( 'NONE', ( #6625 ), #89368, .T. ) ;
#67446=CARTESIAN_POINT ( 'NONE',  ( 5.543860000110784725, 20.76261553274053284, -1.500000000000002220 ) ) ;
#67447=CARTESIAN_POINT ( 'NONE',  ( -86.62287095714999907, -23.96177878511308634, 10.65340807706329507 ) ) ;
#67449=CARTESIAN_POINT ( 'NONE',  ( -18.40674794014382698, -10.35651468716735657, 11.49999999999998934 ) ) ;
#67450=CARTESIAN_POINT ( 'NONE',  ( -99.74569558414813741, -25.22629540225170430, 3.529807444770726388 ) ) ;
#67451=CARTESIAN_POINT ( 'NONE',  ( -64.50991710397673273, -23.96119346886879597, -0.6495511937832134652 ) ) ;
#67452=CARTESIAN_POINT ( 'NONE',  ( -83.54165217798484377, -24.66019654487199375, 8.947790411086122830 ) ) ;
#67454=CARTESIAN_POINT ( 'NONE',  ( -99.41135234760463391, -25.17968299323282011, 3.254169899343974937 ) ) ;
#67455=CARTESIAN_POINT ( 'NONE',  ( 20.41560922187292348, 8.460057656491983380, -1.500000000000002220 ) ) ;
#67456=CARTESIAN_POINT ( 'NONE',  ( -112.6228709571500559, -29.50250786944525672, 11.44777988621622988 ) ) ;
#67458=CARTESIAN_POINT ( 'NONE',  ( -51.91911984596691809, -25.24860220100267938, 5.987871812849870246 ) ) ;
#67459=CARTESIAN_POINT ( 'NONE',  ( -59.22287095715006444, -23.47596703998600276, 11.44779298504227860 ) ) ;
#67463=CARTESIAN_POINT ( 'NONE',  ( -16.21482014894483470, 10.69450053600103345, -1.500000000000002220 ) ) ;
#67464=CARTESIAN_POINT ( 'NONE',  ( 11.27511198983438412, 18.17944245918264912, 11.49999999999998934 ) ) ;
#67466=CARTESIAN_POINT ( 'NONE',  ( -80.62287095715007013, -23.47596703998600631, 11.44779298504227860 ) ) ;
#67468=CARTESIAN_POINT ( 'NONE',  ( -27.68651082257923335, -24.79949475646172630, 7.605672536963987262 ) ) ;
#67469=CARTESIAN_POINT ( 'NONE',  ( 1.383477600506065164, -22.57338898373578218, -1.500000000000002220 ) ) ;
#67473=FACE_OUTER_BOUND ( 'NONE', #80339, .T. ) ;
#67474=CARTESIAN_POINT ( 'NONE',  ( -11.71124675921804403, 15.99993322257668282, 11.49999999999999645 ) ) ;
#67478=ORIENTED_EDGE ( 'NONE', *, *, #36328, .F. ) ;
#67481=CARTESIAN_POINT ( 'NONE',  ( -28.54389657640137656, -24.60093933223103235, 1.825713163565112263 ) ) ;
#67482=CARTESIAN_POINT ( 'NONE',  ( -100.9506922656100727, -25.17353323677711785, 7.008855908370544618 ) ) ;
#67483=CARTESIAN_POINT ( 'NONE',  ( 0.6597851148675514255, -21.60297929554585394, 11.49999999999998934 ) ) ;
#67484=CARTESIAN_POINT ( 'NONE',  ( -49.14425558977711006, -25.27518066829780707, 3.703948608116105490 ) ) ;
#67485=CARTESIAN_POINT ( 'NONE',  ( 17.72857150710123619, 7.855407458714720903, -1.500000000000002220 ) ) ;
#67488=B_SPLINE_CURVE_WITH_KNOTS ( 'NONE', 3,
 ( #11699, #79210, #33052, #56906, #11211, #18324 ),
 .UNSPECIFIED., .F., .F.,
 ( 4, 2, 4 ),
 ( 6.384118678616324667E-06, 0.001386860460828378237, 0.002767336802978140158 ),
 .UNSPECIFIED. ) ;
#67489=CARTESIAN_POINT ( 'NONE',  ( -35.62287095715004881, -24.15431212366388536, -0.2830839119429047757 ) ) ;
#67490=CARTESIAN_POINT ( 'NONE',  ( 9.171884637996585710, -17.55225146786146695, 11.49999999999998934 ) ) ;
#67493=CARTESIAN_POINT ( 'NONE',  ( 18.17922461840205983, -9.147185827878928421, 11.49999999999999645 ) ) ;
#67494=CARTESIAN_POINT ( 'NONE',  ( -80.64675904551151575, -25.20074414427590881, 3.409327697718777195 ) ) ;
#67497=B_SPLINE_CURVE_WITH_KNOTS ( 'NONE', 3,
 ( #83284, #59463, #90406, #51854, #22366, #29993 ),
 .UNSPECIFIED., .F., .F.,
 ( 4, 2, 4 ),
 ( 0.000000000000000000, 0.001380764517854768218, 0.002761529035709536437 ),
 .UNSPECIFIED. ) ;
#67498=ORIENTED_EDGE ( 'NONE', *, *, #31388, .F. ) ;
#67499=CARTESIAN_POINT ( 'NONE',  ( 0.01222413314974575907, -23.20825100983049438, 6.142048374048878046 ) ) ;
#67500=CARTESIAN_POINT ( 'NONE',  ( -111.7814946224345789, -25.29712067403330877, 4.332404411321261861 ) ) ;
#67501=CARTESIAN_POINT ( 'NONE',  ( -64.52287095715010423, -24.66019654487200441, 8.947790411086119278 ) ) ;
#67502=B_SPLINE_CURVE_WITH_KNOTS ( 'NONE', 3,
 ( #43668, #51782, #44673, #14196, #99435, #6597 ),
 .UNSPECIFIED., .F., .F.,
 ( 4, 2, 4 ),
 ( 0.000000000000000000, 0.001380764517854768001, 0.002761529035709536003 ),
 .UNSPECIFIED. ) ;
#67503=CARTESIAN_POINT ( 'NONE',  ( -95.62287095715005592, -25.00158670708909625, 2.256160236439165967 ) ) ;
#67504=LINE ( 'NONE', #36042, #41433 ) ;
#67505=CARTESIAN_POINT ( 'NONE',  ( -20.04763853020464737, 0.9818187932333496404, 11.49999999999998934 ) ) ;
#67509=CARTESIAN_POINT ( 'NONE',  ( -12.44792101662413408, -19.12764231104124946, 11.49999999999999645 ) ) ;
#67510=CARTESIAN_POINT ( 'NONE',  ( -30.47287095715007510, -23.47593906522708451, -1.422904450652597852 ) ) ;
#67512=CARTESIAN_POINT ( 'NONE',  ( -53.55620429048340725, -23.47593901973091235, -1.443836447539009749 ) ) ;
#67514=ADVANCED_FACE ( 'NONE', ( #52310 ), #45198, .T. ) ;
#67516=DIRECTION ( 'NONE',  ( 3.773278334444167608E-23, -1.000000000000000000, 0.000000000000000000 ) ) ;
#67517=CARTESIAN_POINT ( 'NONE',  ( -0.1411031551986380028, 22.44022050402121948, 11.49999999999999645 ) ) ;
#67519=EDGE_LOOP ( 'NONE', ( #70051, #99297, #96949, #53684 ) ) ;
#67520=CARTESIAN_POINT ( 'NONE',  ( 17.42226438573850800, -10.51879874471254261, 11.49999999999998934 ) ) ;
#67522=CARTESIAN_POINT ( 'NONE',  ( 1.269710630819723463, 22.90746787927615102, -1.500000000000002220 ) ) ;
#67523=PLANE ( 'NONE',  #30722 ) ;
#67529=CARTESIAN_POINT ( 'NONE',  ( -77.64776011165024272, -23.48786465467240703, 11.44779295918254647 ) ) ;
#67531=CARTESIAN_POINT ( 'NONE',  ( -15.93125441714207646, -14.09135727244061265, 11.49999999999999645 ) ) ;
#67535=CARTESIAN_POINT ( 'NONE',  ( -21.14055147415990277, -6.693858341896442354, -1.500000000000002220 ) ) ;
#67536=CARTESIAN_POINT ( 'NONE',  ( -13.08992234710881064, 15.94516925376868244, -1.500000000000002220 ) ) ;
#67537=VECTOR ( 'NONE', #79195, 1000.000000000000114 ) ;
#67538=ORIENTED_EDGE ( 'NONE', *, *, #71779, .T. ) ;
#67544=AXIS2_PLACEMENT_3D ( 'NONE', #68804, #82033, #14001 ) ;
#67545=EDGE_LOOP ( 'NONE', ( #65900, #73180, #85481, #53835 ) ) ;
#67546=CARTESIAN_POINT ( 'NONE',  ( -49.52287095715007581, -24.33927499327855060, 9.819080762295818943 ) ) ;
#67547=CARTESIAN_POINT ( 'NONE',  ( -111.5146074832896943, -24.51419770103157703, 9.386484678747162747 ) ) ;
#67548=CARTESIAN_POINT ( 'NONE',  ( -94.52287095715006160, -24.64965694238575011, 8.947790433994196491 ) ) ;
#67549=CARTESIAN_POINT ( 'NONE',  ( -5.109682455881146446, -20.12422286529520932, -1.500000000000002220 ) ) ;
#67551=CARTESIAN_POINT ( 'NONE',  ( 10.83000837110471082, 18.85367679709202804, 11.49999999999999645 ) ) ;
#67553=CARTESIAN_POINT ( 'NONE',  ( -39.44687923781921057, -25.27828342519987359, 4.188173683033348027 ) ) ;
#67555=CARTESIAN_POINT ( 'NONE',  ( -115.5155081638650643, -24.63355581998386157, 0.9682620441943915468 ) ) ;
#67556=CARTESIAN_POINT ( 'NONE',  ( 18.78116726530667080, 12.29669497462397842, 11.49999999999998934 ) ) ;
#67557=AXIS2_PLACEMENT_3D ( 'NONE', #72873, #35310, #50041 ) ;
#67560=CARTESIAN_POINT ( 'NONE',  ( -87.52287095715006160, -23.48783264083352762, -1.443836473376473695 ) ) ;
#67561=DIRECTION ( 'NONE',  ( -3.773278334444166432E-23, 1.000000000000000000, 0.000000000000000000 ) ) ;
#67565=ADVANCED_FACE ( 'NONE', ( #85243 ), #11756, .T. ) ;
#67566=ORIENTED_EDGE ( 'NONE', *, *, #42111, .T. ) ;
#67567=CARTESIAN_POINT ( 'NONE',  ( -20.48789480994130230, 5.740754632170482097, -1.500000000000002220 ) ) ;
#67568=ADVANCED_FACE ( 'NONE', ( #69533 ), #24352, .F. ) ;
#67571=CARTESIAN_POINT ( 'NONE',  ( -18.19455084753484542, -10.52586660885228298, 11.49999999999998934 ) ) ;
#67573=CARTESIAN_POINT ( 'NONE',  ( 22.61316900856233403, 2.020702135111208442, -1.500000000000002220 ) ) ;
#67575=CARTESIAN_POINT ( 'NONE',  ( -29.52287095715006160, -23.38909342368989641, 11.44779306042727285 ) ) ;
#67576=CARTESIAN_POINT ( 'NONE',  ( 21.48171311866277122, -4.276277801222842179, -1.500000000000002220 ) ) ;
#67577=CARTESIAN_POINT ( 'NONE',  ( -87.54532251907512830, -24.51314013834317507, 0.6176544820404262781 ) ) ;
#67579=CARTESIAN_POINT ( 'NONE',  ( -122.6234929911659606, -24.66019654487200086, 8.947790411086113949 ) ) ;
#67580=EDGE_CURVE ( 'NONE', #3446, #1307, #59712, .T. ) ;
#67581=AXIS2_PLACEMENT_3D ( 'NONE', #35489, #89769, #29740 ) ;
#67583=EDGE_LOOP ( 'NONE', ( #28058, #98139, #54520, #51989 ) ) ;
#67584=CARTESIAN_POINT ( 'NONE',  ( -84.55846707206313795, -23.73791477778912551, 11.05961554403170766 ) ) ;
#67587=CARTESIAN_POINT ( 'NONE',  ( -30.60199688435473320, -24.75181118439798311, 1.363349870542264863 ) ) ;
#67588=CARTESIAN_POINT ( 'NONE',  ( 9.380127297304197143, -19.07726845333505494, -1.500000000000002220 ) ) ;
#67589=CARTESIAN_POINT ( 'NONE',  ( -112.5870109292292511, -24.65952944569305316, 1.056160979905707897 ) ) ;
#67590=CARTESIAN_POINT ( 'NONE',  ( -26.80230302508262241, -24.97064477538173222, 2.622372507731231650 ) ) ;
#67591=CARTESIAN_POINT ( 'NONE',  ( -85.63197954799407796, -24.52300882791530157, 0.6510814631126254914 ) ) ;
#67592=CARTESIAN_POINT ( 'NONE',  ( -29.55620429048340725, -23.40356933438083331, -1.443836155048349834 ) ) ;
#67593=B_SPLINE_SURFACE_WITH_KNOTS ( 'NONE', 3, 3, ( 
 ( #63795, #17085, #94711, #34322 ),
 ( #40437, #25194, #79489, #64801 ),
 ( #26205, #56171, #49556, #9976 ),
 ( #2376, #57178, #80485, #33307 ),
 ( #10981, #64295, #72889, #41946 ),
 ( #95218, #65299, #96224, #57666 ),
 ( #88609, #78474, #8974, #67785 ) ),
 .UNSPECIFIED., .F., .F., .F.,
 ( 4, 3, 4 ),
 ( 4, 4 ),
 ( 0.7945040050992246972, 0.8970133687736505657, 0.9995227324480764342 ),
 ( 0.4796158742846823864, 0.4808500213541327395 ),
 .UNSPECIFIED. ) ;
#67596=CARTESIAN_POINT ( 'NONE',  ( -99.96028742912865539, -25.05658428359392076, 7.499825484813623433 ) ) ;
#67597=CARTESIAN_POINT ( 'NONE',  ( 19.42422255247381457, -2.945173967302487039, 11.49999999999999645 ) ) ;
#67598=PLANE ( 'NONE',  #73033 ) ;
#67601=CARTESIAN_POINT ( 'NONE',  ( -69.10880722458374237, -25.29515380318773765, 5.511221748791859554 ) ) ;
#67602=CARTESIAN_POINT ( 'NONE',  ( -99.60228783053516111, -25.31549506111867487, 4.950078004910987595 ) ) ;
#67603=VECTOR ( 'NONE', #21631, 1000.000000000000114 ) ;
#67604=CARTESIAN_POINT ( 'NONE',  ( -25.57898076830435485, -24.90004706754400488, 5.867565877950162267 ) ) ;
#67605=FACE_OUTER_BOUND ( 'NONE', #1918, .T. ) ;
#67606=ADVANCED_FACE ( 'NONE', ( #86749 ), #72540, .F. ) ;
#67607=CARTESIAN_POINT ( 'NONE',  ( 10.64064036176630879, -16.58286410872727146, 11.49999999999998934 ) ) ;
#67608=ORIENTED_EDGE ( 'NONE', *, *, #17923, .F. ) ;
#67610=CARTESIAN_POINT ( 'NONE',  ( -70.62287095715009855, -24.63287334234179937, 0.9662140553045409641 ) ) ;
#67615=CARTESIAN_POINT ( 'NONE',  ( -103.6228709571500559, -24.51387760970723662, 9.387446482453412955 ) ) ;
#67616=CARTESIAN_POINT ( 'NONE',  ( -55.55112771745390177, -24.15503026093912808, -0.2815557561904589168 ) ) ;
#67620=PLANE ( 'NONE',  #34397 ) ;
#67621=CARTESIAN_POINT ( 'NONE',  ( -107.5572310108091187, -23.73766607897672642, -1.055555164236427590 ) ) ;
#67622=CARTESIAN_POINT ( 'NONE',  ( -4.560224734120114753, 19.45435480350565882, -1.500000000000002220 ) ) ;
#67623=DIRECTION ( 'NONE',  ( -3.773278334453079618E-23, 0.9999999999976377785, 2.173523156925979975E-06 ) ) ;
#67624=CARTESIAN_POINT ( 'NONE',  ( -0.01293961071214225038, -22.88248657085181748, 2.995806029868834486 ) ) ;
#67625=VERTEX_POINT ( 'NONE', #40590 ) ;
#67628=CARTESIAN_POINT ( 'NONE',  ( -119.5902202967278072, -24.15543982623907837, -0.2315651400026546569 ) ) ;
#67630=DIRECTION ( 'NONE',  ( -3.773278334444166432E-23, 1.000000000000000000, 0.000000000000000000 ) ) ;
#67631=CARTESIAN_POINT ( 'NONE',  ( -39.51316539375884673, -23.73766607897669800, -1.055555164236461341 ) ) ;
#67632=CARTESIAN_POINT ( 'NONE',  ( -119.6228709571501128, -24.50216790748207529, 0.6166512839542543922 ) ) ;
#67634=B_SPLINE_CURVE_WITH_KNOTS ( 'NONE', 3,
 ( #97356, #80631, #81634, #4518 ),
 .UNSPECIFIED., .F., .F.,
 ( 4, 4 ),
 ( 0.000000000000000000, 9.999999999999592548E-05 ),
 .UNSPECIFIED. ) ;
#67638=CARTESIAN_POINT ( 'NONE',  ( -100.6228709571500559, -29.50249982740957577, 7.747779886224967605 ) ) ;
#67640=CARTESIAN_POINT ( 'NONE',  ( -11.05657426389776354, 17.00066307926000420, -1.500000000000002220 ) ) ;
#67641=CARTESIAN_POINT ( 'NONE',  ( -122.6263427379263220, -23.73766607897671221, -1.055555164236450461 ) ) ;
#67645=ADVANCED_FACE ( 'NONE', ( #33968 ), #94860, .F. ) ;
#67648=ORIENTED_EDGE ( 'NONE', *, *, #9904, .F. ) ;
#67649=PLANE ( 'NONE',  #72879 ) ;
#67650=CARTESIAN_POINT ( 'NONE',  ( -46.52287095715004028, -23.95044443724990657, 10.65354141964648882 ) ) ;
#67651=CARTESIAN_POINT ( 'NONE',  ( 19.36564117097816862, 5.170944958934900804, -1.500000000000002220 ) ) ;
#67652=CARTESIAN_POINT ( 'NONE',  ( 14.88031740681034698, -14.96734982212533183, 11.49999999999999645 ) ) ;
#67656=CARTESIAN_POINT ( 'NONE',  ( -70.49055710964816512, -24.83644354573578283, 8.397322867130098345 ) ) ;
#67657=CARTESIAN_POINT ( 'NONE',  ( -12.21066354923914865, 18.40238043084326591, -1.500000000000002220 ) ) ;
#67658=CARTESIAN_POINT ( 'NONE',  ( -18.81443736134900035, 8.205417114561466718, 11.49999999999998934 ) ) ;
#67659=CARTESIAN_POINT ( 'NONE',  ( -93.55620429048339304, -23.47596703998600631, 11.44779298504227683 ) ) ;
#67667=FACE_OUTER_BOUND ( 'NONE', #41172, .T. ) ;
#67668=CARTESIAN_POINT ( 'NONE',  ( -61.47555956910319708, -25.05987955553484525, 7.435194464380680657 ) ) ;
#67669=CARTESIAN_POINT ( 'NONE',  ( -76.62668118872166190, -24.51314013834316441, 0.6176544820404190617 ) ) ;
#67670=CARTESIAN_POINT ( 'NONE',  ( -9.016818060619870678, -18.48156098877705844, -1.500000000000002220 ) ) ;
#67673=CARTESIAN_POINT ( 'NONE',  ( 21.29926025483437257, -3.289820829717503337, 11.49999999999999645 ) ) ;
#67674=ORIENTED_EDGE ( 'NONE', *, *, #87711, .T. ) ;
#67675=CARTESIAN_POINT ( 'NONE',  ( -99.30689605304669954, -25.29963387158551669, 4.613820302888914426 ) ) ;
#67676=CARTESIAN_POINT ( 'NONE',  ( -129.6228709571500133, -24.34917612406838572, 0.1852690917426697004 ) ) ;
#67677=CARTESIAN_POINT ( 'NONE',  ( -10.28394192611005842, 19.82837715243953625, 11.49999999999998934 ) ) ;
#67678=AXIS2_PLACEMENT_3D ( 'NONE', #50490, #37626, #68583 ) ;
#67680=CARTESIAN_POINT ( 'NONE',  ( -84.64453684150217327, -23.48783264082476308, -1.443836473390094799 ) ) ;
#67681=EDGE_CURVE ( 'NONE', #35091, #85611, #77813, .T. ) ;
#67683=CARTESIAN_POINT ( 'NONE',  ( -43.62287095715004881, -23.47593901973091235, -1.443836447539011525 ) ) ;
#67684=CARTESIAN_POINT ( 'NONE',  ( -35.51857469582687088, -25.00182538069146077, 7.747789668545035369 ) ) ;
#67685=CARTESIAN_POINT ( 'NONE',  ( 20.66465755290784401, -3.126920214821775623, -1.500000000000002220 ) ) ;
#67686=ORIENTED_EDGE ( 'NONE', *, *, #34311, .F. ) ;
#67687=CARTESIAN_POINT ( 'NONE',  ( -86.63552353197610501, -23.96119346886881019, -0.6495511937831902616 ) ) ;
#67689=ORIENTED_EDGE ( 'NONE', *, *, #19991, .F. ) ;
#67691=VERTEX_POINT ( 'NONE', #58027 ) ;
#67692=CARTESIAN_POINT ( 'NONE',  ( -50.90512332773992199, -25.29912375439049654, 4.600680353948681578 ) ) ;
#67693=CARTESIAN_POINT ( 'NONE',  ( -2.902382693073098707, -20.91247731031871382, -1.500000000000002220 ) ) ;
#67697=CARTESIAN_POINT ( 'NONE',  ( -100.6228709571500559, -29.50247984919015209, -1.443849546365050029 ) ) ;
#67698=AXIS2_PLACEMENT_3D ( 'NONE', #57488, #42273, #88424 ) ;
#67699=CARTESIAN_POINT ( 'NONE',  ( -76.62361889982840069, -24.66019654487199375, 8.947790411086119278 ) ) ;
#67700=B_SPLINE_CURVE_WITH_KNOTS ( 'NONE', 3,
 ( #78753, #63067, #70665, #40216 ),
 .UNSPECIFIED., .F., .F.,
 ( 4, 4 ),
 ( 0.000000000000000000, 9.999999999999592548E-05 ),
 .UNSPECIFIED. ) ;
#67701=CARTESIAN_POINT ( 'NONE',  ( -80.48900664166535535, -25.13313949306887807, 7.101635536975466678 ) ) ;
#67702=CARTESIAN_POINT ( 'NONE',  ( -14.02725853290852243, 16.66567569088042688, -1.500000000000002220 ) ) ;
#67703=CARTESIAN_POINT ( 'NONE',  ( -71.22803624472236095, -25.24674067209845418, 4.920688748475479102 ) ) ;
#67704=CARTESIAN_POINT ( 'NONE',  ( -6.278373996654322831, -21.41630973362384083, 11.49999999999999645 ) ) ;
#67706=CARTESIAN_POINT ( 'NONE',  ( -60.62287095715004881, -25.00182538069145011, 7.747789668545098429 ) ) ;
#67710=ORIENTED_EDGE ( 'NONE', *, *, #8433, .T. ) ;
#67711=EDGE_CURVE ( 'NONE', #74791, #27009, #48923, .T. ) ;
#67712=ORIENTED_EDGE ( 'NONE', *, *, #3051, .T. ) ;
#67715=CARTESIAN_POINT ( 'NONE',  ( -101.0859251941938055, -25.16066481202448557, 6.938184544222248284 ) ) ;
#67716=CARTESIAN_POINT ( 'NONE',  ( -78.62287095715005592, -29.50248528299804818, 1.056150453629038477 ) ) ;
#67719=CARTESIAN_POINT ( 'NONE',  ( -8.550378450311910683, 17.38971893761031851, -1.500000000000002220 ) ) ;
#67722=CARTESIAN_POINT ( 'NONE',  ( 2.844571010020486845, -19.19604305453586690, 11.49999999999999645 ) ) ;
#67724=B_SPLINE_CURVE_WITH_KNOTS ( 'NONE', 3,
 ( #22308, #97934, #53286, #29429 ),
 .UNSPECIFIED., .F., .F.,
 ( 4, 4 ),
 ( 0.000000000000000000, 1.000000000000000000 ),
 .UNSPECIFIED. ) ;
#67725=EDGE_LOOP ( 'NONE', ( #69813, #89370, #88356, #77989 ) ) ;
#67727=FACE_OUTER_BOUND ( 'NONE', #25804, .T. ) ;
#67728=AXIS2_PLACEMENT_3D ( 'NONE', #33365, #25760, #42005 ) ;
#67729=CARTESIAN_POINT ( 'NONE',  ( -102.6228709571500275, -23.48783264082478794, -1.443836473390062158 ) ) ;
#67730=DIRECTION ( 'NONE',  ( -3.773278334453079618E-23, 0.9999999999976377785, 2.173523156925979975E-06 ) ) ;
#67731=CARTESIAN_POINT ( 'NONE',  ( 16.02095076306289201, 11.36058263404076030, -1.500000000000002220 ) ) ;
#67733=CARTESIAN_POINT ( 'NONE',  ( -46.49383670590691509, -24.34968618360933235, 0.1864209137778778391 ) ) ;
#67735=CARTESIAN_POINT ( 'NONE',  ( 20.98369277809155165, -4.918611649023987731, 11.49999999999998934 ) ) ;
#67737=CARTESIAN_POINT ( 'NONE',  ( -70.32380231474228083, -25.25639601488366637, 7.101635269074562551 ) ) ;
#67738=FACE_OUTER_BOUND ( 'NONE', #85751, .T. ) ;
#67740=CARTESIAN_POINT ( 'NONE',  ( 20.35648204094723468, -10.72454223111430593, -1.500000000000002220 ) ) ;
#67742=CARTESIAN_POINT ( 'NONE',  ( -101.5084176993576648, -25.27307239909413639, 3.986250617436080113 ) ) ;
#67743=CARTESIAN_POINT ( 'NONE',  ( -83.62287095715005592, -29.50248528299804818, 1.056150453629038477 ) ) ;
#67744=CARTESIAN_POINT ( 'NONE',  ( 4.949566031639514918, 19.51814346981619863, 11.49999999999999645 ) ) ;
#67745=CARTESIAN_POINT ( 'NONE',  ( -109.2412217894342916, -25.28814177081538972, 3.330160904322529536 ) ) ;
#67748=FACE_OUTER_BOUND ( 'NONE', #44193, .T. ) ;
#67749=CARTESIAN_POINT ( 'NONE',  ( -122.5228709571500616, -24.66019654487200441, 8.947790411086112172 ) ) ;
#67750=CARTESIAN_POINT ( 'NONE',  ( -6.239078800006583769, 18.87631364486404806, 11.49999999999998934 ) ) ;
#67751=DIRECTION ( 'NONE',  ( -3.773278334453079618E-23, 0.9999999999976377785, 2.173523156925979975E-06 ) ) ;
#67752=CARTESIAN_POINT ( 'NONE',  ( -6.431973572030615038, 18.70533856667250916, -1.500000000000002220 ) ) ;
#67755=CARTESIAN_POINT ( 'NONE',  ( -73.22287095715006444, -23.47596703998600631, 11.44779298504227860 ) ) ;
#67756=CARTESIAN_POINT ( 'NONE',  ( -37.52287095715008292, -24.51283580621450398, 0.6167428607045408739 ) ) ;
#67757=CARTESIAN_POINT ( 'NONE',  ( 15.34805171112899203, -13.82090413600154299, 11.49999999999999645 ) ) ;
#67758=CARTESIAN_POINT ( 'NONE',  ( -56.55620429048339304, -23.47593901973091235, -1.443836447539007972 ) ) ;
#67761=CARTESIAN_POINT ( 'NONE',  ( -50.05581273115511465, -25.25138681102044913, 5.236521854102218043 ) ) ;
#67762=CARTESIAN_POINT ( 'NONE',  ( -20.99730734726578874, -8.693733401623333634, 11.49999999999999645 ) ) ;
#67764=CARTESIAN_POINT ( 'NONE',  ( -46.62287095715006302, -24.51387760970722240, 9.387446482453421837 ) ) ;
#67768=EDGE_CURVE ( 'NONE', #81257, #50685, #24632, .T. ) ;
#67769=CARTESIAN_POINT ( 'NONE',  ( -9.895454706725905325, 17.58729670687104729, -1.500000000000002220 ) ) ;
#67770=B_SPLINE_CURVE_WITH_KNOTS ( 'NONE', 3,
 ( #22879, #44754, #6676, #75678, #45253, #38122 ),
 .UNSPECIFIED., .F., .F.,
 ( 4, 2, 4 ),
 ( 6.384118695308377748E-06, 0.001386860460836723775, 0.002767336802978138856 ),
 .UNSPECIFIED. ) ;
#67771=CARTESIAN_POINT ( 'NONE',  ( -63.65416434033561899, -23.48783264082475952, -1.443836473390093245 ) ) ;
#67772=EDGE_CURVE ( 'NONE', #56501, #55445, #3736, .T. ) ;
#67773=DIRECTION ( 'NONE',  ( 1.000000000000000000, 3.773278334444167608E-23, 8.201307833595939069E-29 ) ) ;
#67774=B_SPLINE_CURVE_WITH_KNOTS ( 'NONE', 3,
 ( #15713, #76103, #22808, #30939 ),
 .UNSPECIFIED., .F., .F.,
 ( 4, 4 ),
 ( 0.8093576887341661363, 0.8103584357749318290 ),
 .UNSPECIFIED. ) ;
#67776=VERTEX_POINT ( 'NONE', #21306 ) ;
#67777=EDGE_CURVE ( 'NONE', #65243, #55675, #6500, .T. ) ;
#67778=ORIENTED_EDGE ( 'NONE', *, *, #26779, .T. ) ;
#67780=CARTESIAN_POINT ( 'NONE',  ( 9.198035947750891950, -20.93187084735588144, 11.49999999999998934 ) ) ;
#67781=CARTESIAN_POINT ( 'NONE',  ( -29.67002368223832676, -23.41236132725490293, -1.443836171194816886 ) ) ;
#67782=CARTESIAN_POINT ( 'NONE',  ( 17.73057777116804701, 12.32922261165129285, -1.500000000000002220 ) ) ;
#67784=PLANE ( 'NONE',  #56106 ) ;
#67785=CARTESIAN_POINT ( 'NONE',  ( -82.52213977090120522, -23.48786465467241413, 11.44779295918254824 ) ) ;
#67786=CARTESIAN_POINT ( 'NONE',  ( -16.74547196562220464, 15.07928529822544661, 11.49999999999999645 ) ) ;
#67787=ORIENTED_EDGE ( 'NONE', *, *, #72263, .T. ) ;
#67789=CARTESIAN_POINT ( 'NONE',  ( -1.351711525931510449, 21.94731587555429186, -1.500000000000002220 ) ) ;
#67790=DIRECTION ( 'NONE',  ( -3.773278334453079030E-23, 0.9999999999976377785, 2.173523156925979128E-06 ) ) ;
#67791=FACE_OUTER_BOUND ( 'NONE', #6858, .T. ) ;
#67792=ORIENTED_EDGE ( 'NONE', *, *, #70192, .T. ) ;
#67794=CARTESIAN_POINT ( 'NONE',  ( -90.63673542715442011, -24.15602025860896873, 10.28564288303535434 ) ) ;
#67796=CARTESIAN_POINT ( 'NONE',  ( -29.52287095715007581, -24.57618165405973087, 1.056161296257514870 ) ) ;
#67800=DIRECTION ( 'NONE',  ( -3.773278334444166432E-23, 1.000000000000000000, 0.000000000000000000 ) ) ;
#67801=CARTESIAN_POINT ( 'NONE',  ( -57.52207148937385739, -23.48783264082477018, -1.443836473390095243 ) ) ;
#67802=CARTESIAN_POINT ( 'NONE',  ( -10.01004151551622456, -17.79114453763541093, -1.500000000000002220 ) ) ;
#67803=EDGE_CURVE ( 'NONE', #21715, #46174, #29424, .T. ) ;
#67806=CARTESIAN_POINT ( 'NONE',  ( -99.52287095715001897, -24.35013146730204525, 9.818937971375097717 ) ) ;
#67809=EDGE_CURVE ( 'NONE', #37373, #70639, #56114, .T. ) ;
#67810=EDGE_LOOP ( 'NONE', ( #5997, #76029, #50987, #46411 ) ) ;
#67811=CARTESIAN_POINT ( 'NONE',  ( -51.52287095715006870, -29.50250243563736774, 8.947779886222146928 ) ) ;
#67812=CARTESIAN_POINT ( 'NONE',  ( -27.75512851621423138, -25.26248076641628515, 8.250985936982687008 ) ) ;
#67813=CARTESIAN_POINT ( 'NONE',  ( 18.03836333725549324, -10.36167025447706713, 11.49999999999998934 ) ) ;
#67817=B_SPLINE_SURFACE_WITH_KNOTS ( 'NONE', 3, 1, ( 
 ( #4056, #10164 ),
 ( #12148, #48744 ),
 ( #2067, #18276 ),
 ( #33006, #34505 ),
 ( #63981, #35000 ),
 ( #49746, #41124 ),
 ( #42135, #27392 ) ),
 .UNSPECIFIED., .F., .F., .F.,
 ( 4, 1, 1, 1, 4 ),
 ( 2, 2 ),
 ( 0.000000000000000000, 0.2750683690187516461, 0.5329014600899387721, 0.7739734595924534499, 1.000000000000000000 ),
 ( 0.000000000000000000, 1.000000000000000000 ),
 .UNSPECIFIED. ) ;
#67819=ORIENTED_EDGE ( 'NONE', *, *, #8293, .T. ) ;
#67820=EDGE_LOOP ( 'NONE', ( #56005, #58152, #28809, #67440 ) ) ;
#67822=CARTESIAN_POINT ( 'NONE',  ( -116.7735416517568297, -25.27125674707836822, 4.078964885054422673 ) ) ;
#67823=CARTESIAN_POINT ( 'NONE',  ( -86.52287095715007581, -23.94994826722565406, -0.6494450866342726947 ) ) ;
#67824=CARTESIAN_POINT ( 'NONE',  ( -100.5895376238167245, -25.00182538069145721, 7.747789668545099317 ) ) ;
#67825=CARTESIAN_POINT ( 'NONE',  ( -8.904070064990065703, -20.24664451029508783, 11.49999999999999645 ) ) ;
#67826=ORIENTED_EDGE ( 'NONE', *, *, #78882, .T. ) ;
#67827=CARTESIAN_POINT ( 'NONE',  ( -108.5552614013656978, -23.96119346886881729, -0.6495511937831862648 ) ) ;
#67828=CARTESIAN_POINT ( 'NONE',  ( -22.13905560727926414, 4.690293145198261904, -1.500000000000002220 ) ) ;
#67829=VECTOR ( 'NONE', #74839, 1000.000000000000114 ) ;
#67833=EDGE_LOOP ( 'NONE', ( #68296, #11489, #51214, #59078 ) ) ;
#67834=PLANE ( 'NONE',  #93629 ) ;
#67835=EDGE_CURVE ( 'NONE', #48827, #40589, #65840, .T. ) ;
#67836=CARTESIAN_POINT ( 'NONE',  ( -18.49208213979201076, -7.923680710433813168, 11.49999999999998934 ) ) ;
#67837=CARTESIAN_POINT ( 'NONE',  ( -57.61198011476029279, -23.48786465467241058, 11.44779295918254647 ) ) ;
#67838=ORIENTED_EDGE ( 'NONE', *, *, #71358, .F. ) ;
#67841=CARTESIAN_POINT ( 'NONE',  ( 20.56042274393015035, -8.519965759701490171, -1.500000000000002220 ) ) ;
#67845=DIRECTION ( 'NONE',  ( -0.000000000000000000, 2.173523156925979552E-06, -0.9999999999976378895 ) ) ;
#67848=CARTESIAN_POINT ( 'NONE',  ( -9.627943313441900131, 16.98966435471970726, -1.500000000000002220 ) ) ;
#67849=VECTOR ( 'NONE', #24552, 1000.000000000000114 ) ;
#67850=CARTESIAN_POINT ( 'NONE',  ( 1.049947104896167049, -21.43676768134831434, 11.49999999999998934 ) ) ;
#67854=CARTESIAN_POINT ( 'NONE',  ( 19.59772090806136902, -11.66877021596143926, -1.500000000000002220 ) ) ;
#67856=CARTESIAN_POINT ( 'NONE',  ( -96.50857322515494729, -24.51419770103159834, 9.386484678747169852 ) ) ;
#67858=CARTESIAN_POINT ( 'NONE',  ( -15.89961544564849305, 12.09337254111102844, 11.49999999999999645 ) ) ;
#67860=CARTESIAN_POINT ( 'NONE',  ( -74.49972297989059200, -24.51419770103157703, 9.386484678747164523 ) ) ;
#67863=CARTESIAN_POINT ( 'NONE',  ( -110.6228709571500559, -29.50248528299804818, 1.056150453629043584 ) ) ;
#67865=CARTESIAN_POINT ( 'NONE',  ( 21.72137571921558319, 1.130696696492564213, -1.500000000000002220 ) ) ;
#67867=CARTESIAN_POINT ( 'NONE',  ( 3.881049643139886207, -19.21785841795820104, -1.500000000000002220 ) ) ;
#67868=CARTESIAN_POINT ( 'NONE',  ( -99.46032996850638597, -25.20155714560419469, 6.668840158564011134 ) ) ;
#67873=CARTESIAN_POINT ( 'NONE',  ( -6.383830130275963910, 19.51498944528526991, 11.49999999999999645 ) ) ;
#67875=CARTESIAN_POINT ( 'NONE',  ( -61.24303164512834030, -25.04307381209219230, 7.563174986197129357 ) ) ;
#67876=ORIENTED_EDGE ( 'NONE', *, *, #53001, .F. ) ;
#67878=CARTESIAN_POINT ( 'NONE',  ( -40.25588136632453740, -25.18430874478563197, 3.308432125291594250 ) ) ;
#67880=CARTESIAN_POINT ( 'NONE',  ( -42.62287095715004881, -29.50250243563736774, 8.947779886222148704 ) ) ;
#67881=EDGE_CURVE ( 'NONE', #98594, #99101, #51250, .T. ) ;
#67883=B_SPLINE_CURVE_WITH_KNOTS ( 'NONE', 3,
 ( #21618, #15013, #30237, #68813 ),
 .UNSPECIFIED., .F., .F.,
 ( 4, 4 ),
 ( 0.000000000000000000, 1.000000000000000000 ),
 .UNSPECIFIED. ) ;
#67884=B_SPLINE_CURVE_WITH_KNOTS ( 'NONE', 3,
 ( #58685, #4899, #11503, #42482 ),
 .UNSPECIFIED., .F., .F.,
 ( 4, 4 ),
 ( 0.000000000000000000, 0.0001000000000000028644 ),
 .UNSPECIFIED. ) ;
#67887=ORIENTED_EDGE ( 'NONE', *, *, #15400, .F. ) ;
#67888=CARTESIAN_POINT ( 'NONE',  ( -119.6228709571500559, -23.48783264082479150, -1.443836473390058384 ) ) ;
#67890=EDGE_CURVE ( 'NONE', #72942, #7077, #67089, .T. ) ;
#67891=CARTESIAN_POINT ( 'NONE',  ( 18.09022303007301247, 14.20294132079179938, 11.49999999999999645 ) ) ;
#67892=CARTESIAN_POINT ( 'NONE',  ( -20.44213351528904354, 10.05872170072450977, -1.500000000000002220 ) ) ;
#67893=CARTESIAN_POINT ( 'NONE',  ( -70.66110687620329145, -25.31517380081856672, 4.882286551243335992 ) ) ;
#67898=CARTESIAN_POINT ( 'NONE',  ( -45.62287095715004881, -29.50249982740957577, 7.747779886224967605 ) ) ;
#67900=CARTESIAN_POINT ( 'NONE',  ( -69.55620429048337883, -24.64898659630528854, 1.056161002820824368 ) ) ;
#67901=CARTESIAN_POINT ( 'NONE',  ( 21.88901064076550185, 0.7357440816682787599, -1.500000000000002220 ) ) ;
#67902=FACE_OUTER_BOUND ( 'NONE', #38682, .T. ) ;
#67904=CARTESIAN_POINT ( 'NONE',  ( -33.52287095715004739, -23.96177878511307924, 10.65340807706330750 ) ) ;
#67905=CARTESIAN_POINT ( 'NONE',  ( -78.59599014444141574, -23.96119346886880308, -0.6495511937832113558 ) ) ;
#67906=DIRECTION ( 'NONE',  ( -3.773278334444166432E-23, 1.000000000000000000, 0.000000000000000000 ) ) ;
#67908=VERTEX_POINT ( 'NONE', #45171 ) ;
#67910=CARTESIAN_POINT ( 'NONE',  ( -2.750569593922542300, -20.27526743851804625, 11.49999999999998934 ) ) ;
#67912=EDGE_LOOP ( 'NONE', ( #22328, #23596, #28721, #53540 ) ) ;
#67913=EDGE_LOOP ( 'NONE', ( #48463, #11558, #14258, #74669 ) ) ;
#67914=ORIENTED_EDGE ( 'NONE', *, *, #44290, .F. ) ;
#67915=CARTESIAN_POINT ( 'NONE',  ( -20.34888222059871410, 10.79260868881566715, 11.49999999999998934 ) ) ;
#67916=DIRECTION ( 'NONE',  ( 0.000000000000000000, -0.9999999999976377785, -2.173523156925979975E-06 ) ) ;
#67917=CARTESIAN_POINT ( 'NONE',  ( -14.69473627950705108, 13.90061564059656440, -1.500000000000002220 ) ) ;
#67918=ORIENTED_EDGE ( 'NONE', *, *, #77743, .F. ) ;
#67919=CARTESIAN_POINT ( 'NONE',  ( -27.15236911514251972, -24.75132242458699849, 7.636915180611342002 ) ) ;
#67920=CARTESIAN_POINT ( 'NONE',  ( -40.58132354090890459, -25.30363535146268816, 5.541646066808135096 ) ) ;
#67921=CARTESIAN_POINT ( 'NONE',  ( -47.52287095715006160, -23.48783264083458988, -1.443836473374825236 ) ) ;
#67922=CARTESIAN_POINT ( 'NONE',  ( -70.54351358342104561, -24.52300882791528380, 0.6510814631126248253 ) ) ;
#67923=CARTESIAN_POINT ( 'NONE',  ( -11.90495014755217618, 17.82271480561356469, 11.49999999999999645 ) ) ;
#67924=ORIENTED_EDGE ( 'NONE', *, *, #53445, .F. ) ;
#67925=B_SPLINE_CURVE_WITH_KNOTS ( 'NONE', 3,
 ( #85288, #95412, #96412, #95910, #56871, #33018 ),
 .UNSPECIFIED., .F., .F.,
 ( 4, 2, 4 ),
 ( 6.391158118969315506E-06, 0.001387004593080790266, 0.002767618028042611537 ),
 .UNSPECIFIED. ) ;
#67927=CARTESIAN_POINT ( 'NONE',  ( -41.59371986446371494, -24.15543982623907127, -0.2315651400026566831 ) ) ;
#67928=ORIENTED_EDGE ( 'NONE', *, *, #25599, .T. ) ;
#67929=B_SPLINE_CURVE_WITH_KNOTS ( 'NONE', 3,
 ( #95121, #56579, #34231, #79887, #34723, #65204 ),
 .UNSPECIFIED., .F., .F.,
 ( 4, 2, 4 ),
 ( 0.000000000000000000, 0.001380764517853247733, 0.002761529035706495466 ),
 .UNSPECIFIED. ) ;
#67930=CARTESIAN_POINT ( 'NONE',  ( -19.01758589260300525, -8.224767016273846210, -1.500000000000002220 ) ) ;
#67931=VERTEX_POINT ( 'NONE', #22299 ) ;
#67932=CARTESIAN_POINT ( 'NONE',  ( -91.52287095715011844, -24.51387760970726504, 9.387446482453416507 ) ) ;
#67935=VERTEX_POINT ( 'NONE', #8599 ) ;
#67936=CARTESIAN_POINT ( 'NONE',  ( 19.54352652498339182, 7.673529024697476331, -1.500000000000002220 ) ) ;
#67937=CARTESIAN_POINT ( 'NONE',  ( -19.92591009635028243, 9.278653061003369729, 11.49999999999999645 ) ) ;
#67939=CARTESIAN_POINT ( 'NONE',  ( 15.74396088501716839, 16.14010210793005839, 11.49999999999998934 ) ) ;
#67940=CARTESIAN_POINT ( 'NONE',  ( -20.92093621315066443, -1.481899440790641842, -1.500000000000002220 ) ) ;
#67941=CARTESIAN_POINT ( 'NONE',  ( -48.62287095715004881, -23.48783264082478439, -1.443836473390070596 ) ) ;
#67947=CARTESIAN_POINT ( 'NONE',  ( -66.54902258912107982, -24.15543982623906771, -0.2315651400026687845 ) ) ;
#67949=CARTESIAN_POINT ( 'NONE',  ( 8.900169022907615357, -19.58186849131130813, -1.500000000000002220 ) ) ;
#67951=CARTESIAN_POINT ( 'NONE',  ( -121.5895376238167103, -24.66019654487200086, 8.947790411086115725 ) ) ;
#67953=CARTESIAN_POINT ( 'NONE',  ( 14.88031740681034698, -14.96734982212533183, -1.500000000000002220 ) ) ;
#67954=FACE_OUTER_BOUND ( 'NONE', #2743, .T. ) ;
#67955=DIRECTION ( 'NONE',  ( -0.8244855201331809935, 1.229959914849042681E-06, -0.5658830507173768787 ) ) ;
#67957=LINE ( 'NONE', #66484, #41028 ) ;
#67958=CARTESIAN_POINT ( 'NONE',  ( -100.1148124853301340, -25.11623808430151072, 2.865158905384864951 ) ) ;
#67959=CARTESIAN_POINT ( 'NONE',  ( 12.17348956504948987, -18.45705692928949659, -1.500000000000002220 ) ) ;
#67961=ORIENTED_EDGE ( 'NONE', *, *, #80360, .F. ) ;
#67962=CARTESIAN_POINT ( 'NONE',  ( -56.52287095715008292, -24.50321055353803956, 9.387540953477522265 ) ) ;
#67963=CARTESIAN_POINT ( 'NONE',  ( -79.62287095715005592, -24.33832256527048798, 0.1851278514138599840 ) ) ;
#67964=CARTESIAN_POINT ( 'NONE',  ( -99.52287095715006160, -23.47596703998600631, 11.44779298504228215 ) ) ;
#67965=B_SPLINE_CURVE_WITH_KNOTS ( 'NONE', 3,
 ( #93678, #16051, #6949, #62251, #37903, #15554 ),
 .UNSPECIFIED., .F., .F.,
 ( 4, 2, 4 ),
 ( 1.570887131794176733E-05, 0.001396322306279756519, 0.002776935741241571502 ),
 .UNSPECIFIED. ) ;
#67966=VECTOR ( 'NONE', #87890, 1000.000000000000114 ) ;
#67967=CARTESIAN_POINT ( 'NONE',  ( -97.52287095715004739, -24.50321055353804667, 9.387540953477522265 ) ) ;
#67969=CARTESIAN_POINT ( 'NONE',  ( -9.780116039169133302, 16.78644576961053048, 11.49999999999998934 ) ) ;
#67971=CARTESIAN_POINT ( 'NONE',  ( 11.27511198983438412, 18.17944245918264912, -1.500000000000002220 ) ) ;
#67973=CARTESIAN_POINT ( 'NONE',  ( -91.16165857266686601, -25.26877915520014639, 5.947789088310639904 ) ) ;
#67974=CARTESIAN_POINT ( 'NONE',  ( -40.52287095715005449, -25.00158670708908915, 2.256160236439166411 ) ) ;
#67976=CARTESIAN_POINT ( 'NONE',  ( 22.15051849217804403, -4.756829024181505439, -1.500000000000002220 ) ) ;
#67978=ORIENTED_EDGE ( 'NONE', *, *, #87470, .T. ) ;
#67979=CARTESIAN_POINT ( 'NONE',  ( -119.5228709571500474, -23.47593901973090524, -1.443836447538996204 ) ) ;
#67980=DIRECTION ( 'NONE',  ( -1.000000000000000000, -3.773278334444166432E-23, -8.201307841325785021E-29 ) ) ;
#67981=CARTESIAN_POINT ( 'NONE',  ( -1.996473883165060581, 19.68112600131995293, 11.49999999999999645 ) ) ;
#67982=CARTESIAN_POINT ( 'NONE',  ( -67.52287095715009002, -23.48783264082477018, -1.443836473390090802 ) ) ;
#67983=ORIENTED_EDGE ( 'NONE', *, *, #17885, .T. ) ;
#67984=CARTESIAN_POINT ( 'NONE',  ( -59.52287095715008292, -23.72747288104470798, -1.053458166803227014 ) ) ;
#67985=DIRECTION ( 'NONE',  ( 0.000000000000000000, -2.173523156925979552E-06, 0.9999999999976378895 ) ) ;
#67986=CARTESIAN_POINT ( 'NONE',  ( -5.517532219241116032, 20.92096086382833064, 11.49999999999998934 ) ) ;
#67987=CARTESIAN_POINT ( 'NONE',  ( -99.62287095715007013, -24.34917612406838217, 0.1852690917426680350 ) ) ;
#67988=CARTESIAN_POINT ( 'NONE',  ( 18.67713048845720181, -5.233370074711279685, -1.500000000000002220 ) ) ;
#67989=CARTESIAN_POINT ( 'NONE',  ( -61.62287095715007723, -24.34917612406837506, 0.1852690917426614847 ) ) ;
#67991=CARTESIAN_POINT ( 'NONE',  ( -4.105667982141768313, -19.37954422259287668, 11.49999999999998934 ) ) ;
#67992=ORIENTED_EDGE ( 'NONE', *, *, #50823, .F. ) ;
#67993=CARTESIAN_POINT ( 'NONE',  ( 18.91379238805564356, 7.493326543281090935, 11.49999999999999645 ) ) ;
#67994=CARTESIAN_POINT ( 'NONE',  ( -111.5228709571500758, -24.66019654487200441, 8.947790411086108620 ) ) ;
#67996=ORIENTED_EDGE ( 'NONE', *, *, #7994, .T. ) ;
#67998=CARTESIAN_POINT ( 'NONE',  ( -102.6311381732150494, -23.96169478059713498, 10.65365249895717881 ) ) ;
#68000=DIRECTION ( 'NONE',  ( -3.773278334453080206E-23, 0.9999999999976377785, 2.173523156925979975E-06 ) ) ;
#68001=CARTESIAN_POINT ( 'NONE',  ( -47.58953762381673158, -23.47593901973091235, -1.443836447539009749 ) ) ;
#68002=CARTESIAN_POINT ( 'NONE',  ( -51.52764846858840997, -25.24768739062223943, 6.187572788000800017 ) ) ;
#68003=CARTESIAN_POINT ( 'NONE',  ( -18.81522532469529452, 6.996975221643539911, -1.500000000000002220 ) ) ;
#68004=CARTESIAN_POINT ( 'NONE',  ( -120.6228709571500559, -25.00182538069145721, 7.747789668545100206 ) ) ;
#68005=ORIENTED_EDGE ( 'NONE', *, *, #35685, .T. ) ;
#68007=CARTESIAN_POINT ( 'NONE',  ( -10.93939140624874007, -20.02795264745160608, 11.49999999999999645 ) ) ;
#68008=CARTESIAN_POINT ( 'NONE',  ( -49.57368764975930731, -25.26258781768282446, 4.259412078242385213 ) ) ;
#68011=DIRECTION ( 'NONE',  ( -3.773278334453079618E-23, 0.9999999999976377785, 2.173523156925979975E-06 ) ) ;
#68014=B_SPLINE_CURVE_WITH_KNOTS ( 'NONE', 3,
 ( #80537, #72440, #71436, #11031 ),
 .UNSPECIFIED., .F., .F.,
 ( 4, 4 ),
 ( 0.7092829846576129693, 0.7102837316983785509 ),
 .UNSPECIFIED. ) ;
#68016=CARTESIAN_POINT ( 'NONE',  ( -80.62287095715005592, -29.50249982740957577, 7.747779886224967605 ) ) ;
#68018=ORIENTED_EDGE ( 'NONE', *, *, #39669, .F. ) ;
#68020=CARTESIAN_POINT ( 'NONE',  ( 15.61528876134825161, -13.05345633644532732, 11.49999999999998934 ) ) ;
#68022=EDGE_CURVE ( 'NONE', #55708, #47794, #64571, .T. ) ;
#68023=CARTESIAN_POINT ( 'NONE',  ( 1.269710630819723463, 22.90746787927615102, 11.49999999999998934 ) ) ;
#68025=VERTEX_POINT ( 'NONE', #478 ) ;
#68027=CARTESIAN_POINT ( 'NONE',  ( -101.4435148696508406, -25.21059354442303047, 6.520239176572899531 ) ) ;
#68028=CARTESIAN_POINT ( 'NONE',  ( -67.52287095715007581, -23.72773821059536559, 11.05748984161097326 ) ) ;
#68029=VECTOR ( 'NONE', #127, 1000.000000000000114 ) ;
#68030=CARTESIAN_POINT ( 'NONE',  ( -51.58226167061351219, -24.51419770103156637, 9.386484678747176957 ) ) ;
#68031=CARTESIAN_POINT ( 'NONE',  ( 4.782327729912362990, -20.71560727227588927, 11.49999999999999645 ) ) ;
#68032=ORIENTED_EDGE ( 'NONE', *, *, #1858, .T. ) ;
#68033=AXIS2_PLACEMENT_3D ( 'NONE', #34538, #73597, #64516 ) ;
#68035=CARTESIAN_POINT ( 'NONE',  ( 17.07819277939130842, -14.19623557145530057, -1.500000000000002220 ) ) ;
#68036=CARTESIAN_POINT ( 'NONE',  ( -9.157874670058189892, -18.46812626297970539, -1.500000000000002220 ) ) ;
#68038=ORIENTED_EDGE ( 'NONE', *, *, #27799, .T. ) ;
#68041=CARTESIAN_POINT ( 'NONE',  ( -56.62287095715006302, -23.73907113216990794, -1.053371485793233031 ) ) ;
#68045=CARTESIAN_POINT ( 'NONE',  ( -75.62287095715005592, -23.47596703998600631, 11.44779298504227860 ) ) ;
#68047=CARTESIAN_POINT ( 'NONE',  ( 19.40640353424967302, -7.489167304209242815, -1.500000000000002220 ) ) ;
#68048=CARTESIAN_POINT ( 'NONE',  ( 15.22768361601695020, -15.61070304372801587, 11.49999999999999645 ) ) ;
#68049=CARTESIAN_POINT ( 'NONE',  ( -51.91081924717653351, -25.22346074172688901, 6.413989918693766334 ) ) ;
#68050=LINE ( 'NONE', #52819, #43424 ) ;
#68051=CARTESIAN_POINT ( 'NONE',  ( -17.93832129671990572, 13.47109510200611560, -1.500000000000002220 ) ) ;
#68052=CARTESIAN_POINT ( 'NONE',  ( -49.10457154551148307, -29.50249168100820896, 3.999763059310747160 ) ) ;
#68054=EDGE_CURVE ( 'NONE', #96886, #30238, #42813, .T. ) ;
#68055=B_SPLINE_CURVE_WITH_KNOTS ( 'NONE', 3,
 ( #59216, #27762, #66349, #4437, #99257, #74916 ),
 .UNSPECIFIED., .F., .F.,
 ( 4, 2, 4 ),
 ( 0.000000000000000000, 0.001380901958385387894, 0.002761803916770775788 ),
 .UNSPECIFIED. ) ;
#68056=CARTESIAN_POINT ( 'NONE',  ( -71.69006450592775082, -25.27819024002308268, 5.957498326979273173 ) ) ;
#68062=EDGE_LOOP ( 'NONE', ( #12236, #65505, #65209, #33621 ) ) ;
#68063=CARTESIAN_POINT ( 'NONE',  ( 20.93798385506118365, 3.901641247904229282, -1.500000000000002220 ) ) ;
#68066=CARTESIAN_POINT ( 'NONE',  ( -20.81348254183067681, -2.960215062046979373, 11.49999999999998934 ) ) ;
#68067=CARTESIAN_POINT ( 'NONE',  ( -38.52287095715006870, -23.47596703998600631, 11.44779298504229281 ) ) ;
#68068=CARTESIAN_POINT ( 'NONE',  ( -41.44993916608342488, -25.18431026911753889, 4.009750576414989887 ) ) ;
#68069=CARTESIAN_POINT ( 'NONE',  ( -32.07722060962682775, -29.50248914092071928, 2.831113219569932227 ) ) ;
#68070=CARTESIAN_POINT ( 'NONE',  ( -12.72821696145241255, -17.84489267850806726, -1.500000000000002220 ) ) ;
#68071=CARTESIAN_POINT ( 'NONE',  ( -87.50497043089684723, -24.51314013834317507, 0.6176544820404262781 ) ) ;
#68073=CARTESIAN_POINT ( 'NONE',  ( -122.6271177707151878, -23.48786465467241769, 11.44779295918253581 ) ) ;
#68074=CARTESIAN_POINT ( 'NONE',  ( -120.5228709571500190, -24.91544648472626378, 1.928969306349433976 ) ) ;
#68075=CARTESIAN_POINT ( 'NONE',  ( -41.62287095715006302, -24.65952944569303895, 1.056160979905692576 ) ) ;
#68076=CARTESIAN_POINT ( 'NONE',  ( -30.63910746512184247, -23.78113234500525408, 10.97511746239722186 ) ) ;
#68077=CARTESIAN_POINT ( 'NONE',  ( 19.98943718749924159, -7.363913660680385220, 11.49999999999998934 ) ) ;
#68078=FACE_OUTER_BOUND ( 'NONE', #12903, .T. ) ;
#68082=CARTESIAN_POINT ( 'NONE',  ( -70.52287095715009002, -23.84047902841604838, -0.8780736468305397890 ) ) ;
#68084=CARTESIAN_POINT ( 'NONE',  ( -6.794891441663577503, 21.43730618243864683, -1.500000000000002220 ) ) ;
#68085=CARTESIAN_POINT ( 'NONE',  ( -108.8781268588537046, -25.11552134530501590, 2.805129186380272088 ) ) ;
#68086=ORIENTED_EDGE ( 'NONE', *, *, #51502, .F. ) ;
#68087=CARTESIAN_POINT ( 'NONE',  ( -30.47287095715008576, -23.47593902499770380, -1.441415665115638456 ) ) ;
#68088=CARTESIAN_POINT ( 'NONE',  ( 10.71975780190685690, -16.47196428025586812, 11.49999999999999645 ) ) ;
#68091=B_SPLINE_CURVE_WITH_KNOTS ( 'NONE', 3,
 ( #596, #46780, #38657, #84831, #16322, #14810, #100034, #31547 ),
 .UNSPECIFIED., .F., .F.,
 ( 4, 2, 2, 4 ),
 ( -0.001224873891641421308, -0.0002244903592271061104, 0.0007758931731872090870, 0.002776660238015835145 ),
 .UNSPECIFIED. ) ;
#68092=CARTESIAN_POINT ( 'NONE',  ( -89.81226385320381667, -25.26877915520014994, 5.947789088310639904 ) ) ;
#68093=ORIENTED_EDGE ( 'NONE', *, *, #88499, .T. ) ;
#68094=CARTESIAN_POINT ( 'NONE',  ( -69.26415293485048608, -25.30211383818459581, 5.299568534518257046 ) ) ;
#68095=CARTESIAN_POINT ( 'NONE',  ( -36.52287095715009002, -24.33927499327854349, 9.819080762295813614 ) ) ;
#68097=CARTESIAN_POINT ( 'NONE',  ( -100.0218067620262303, -25.25095795709099278, 5.284572167519165475 ) ) ;
#68099=CARTESIAN_POINT ( 'NONE',  ( -10.80270875523330965, -16.48872379891551532, 11.49999999999998934 ) ) ;
#68101=ORIENTED_EDGE ( 'NONE', *, *, #2132, .T. ) ;
#68104=CARTESIAN_POINT ( 'NONE',  ( -28.62287095715004881, -23.31954350884483773, -1.443835782653508426 ) ) ;
#68105=B_SPLINE_CURVE_WITH_KNOTS ( 'NONE', 3,
 ( #53977, #68697, #30618, #69694 ),
 .UNSPECIFIED., .F., .F.,
 ( 4, 4 ),
 ( 0.04052894072451945079, 0.04953537199663500534 ),
 .UNSPECIFIED. ) ;
#68110=CARTESIAN_POINT ( 'NONE',  ( -87.55620429048339304, -24.64965694238575011, 8.947790433994194714 ) ) ;
#68111=CARTESIAN_POINT ( 'NONE',  ( -90.55620429048340725, -23.48786465467241413, 11.44779295918254647 ) ) ;
#68112=CARTESIAN_POINT ( 'NONE',  ( -118.5911711821453451, -23.96119346886881374, -0.6495511937832023630 ) ) ;
#68114=CARTESIAN_POINT ( 'NONE',  ( -69.79628282111092119, -25.24515073828506928, 5.458995855196883795 ) ) ;
#68115=CARTESIAN_POINT ( 'NONE',  ( -112.5228709571500616, -24.33832256527048798, 0.1851278514138649522 ) ) ;
#68116=CARTESIAN_POINT ( 'NONE',  ( -4.560224734120114753, 19.45435480350565882, 11.49999999999998934 ) ) ;
#68118=CARTESIAN_POINT ( 'NONE',  ( -45.55620429048340014, -23.47593901973091235, -1.443836447539009749 ) ) ;
#68119=CARTESIAN_POINT ( 'NONE',  ( -45.53131674849007027, -24.73531770709094957, 8.716586749053515604 ) ) ;
#68123=CARTESIAN_POINT ( 'NONE',  ( -80.53951186416253449, -24.83644354573579349, 8.397322867130094792 ) ) ;
#68124=CARTESIAN_POINT ( 'NONE',  ( -81.62287095715005592, -23.48783264082478794, -1.443836473390065711 ) ) ;
#68125=CARTESIAN_POINT ( 'NONE',  ( -107.5895376238167245, -24.66019654487199375, 8.947790411086121054 ) ) ;
#68127=CARTESIAN_POINT ( 'NONE',  ( -97.55620429048339304, -24.65952944569304606, 1.056160979905701236 ) ) ;
#68132=CARTESIAN_POINT ( 'NONE',  ( -19.34540493331696354, 6.066486871809979142, -1.500000000000002220 ) ) ;
#68134=EDGE_CURVE ( 'NONE', #84065, #26881, #60964, .T. ) ;
#68136=CARTESIAN_POINT ( 'NONE',  ( -76.62287095715002749, -23.73907113216991860, -1.053371485793229034 ) ) ;
#68140=CARTESIAN_POINT ( 'NONE',  ( 4.949566031639514918, 19.51814346981619863, -1.500000000000002220 ) ) ;
#68141=CARTESIAN_POINT ( 'NONE',  ( 1.225302832070333636, 21.05158420706169764, 11.49999999999999645 ) ) ;
#68143=CARTESIAN_POINT ( 'NONE',  ( 17.94654606563480215, 12.89224558282342947, 11.49999999999998934 ) ) ;
#68144=VECTOR ( 'NONE', #53586, 1000.000000000000114 ) ;
#68145=CARTESIAN_POINT ( 'NONE',  ( 19.76637988705548210, 5.604140092158477415, 11.49999999999998934 ) ) ;
#68146=CARTESIAN_POINT ( 'NONE',  ( -96.52287095715006160, -24.64898659630528499, 1.056161002820829697 ) ) ;
#68147=PLANE ( 'NONE',  #53316 ) ;
#68150=ORIENTED_EDGE ( 'NONE', *, *, #19531, .T. ) ;
#68154=EDGE_LOOP ( 'NONE', ( #13318, #59441, #35176, #31874 ) ) ;
#68155=CARTESIAN_POINT ( 'NONE',  ( -118.6228709571500559, -23.47593901973091235, -1.443836447538997536 ) ) ;
#68157=CARTESIAN_POINT ( 'NONE',  ( -76.64295899339111884, -23.73766607897670866, -1.055555164236452681 ) ) ;
#68158=CARTESIAN_POINT ( 'NONE',  ( -10.41206725544052780, -17.73373708237225799, -1.500000000000002220 ) ) ;
#68159=CARTESIAN_POINT ( 'NONE',  ( -4.285004571687458963, -21.18589511591401831, 11.49999999999999645 ) ) ;
#68161=PLANE ( 'NONE',  #4527 ) ;
#68162=DIRECTION ( 'NONE',  ( 3.773278334444167608E-23, -1.000000000000000000, 0.000000000000000000 ) ) ;
#68163=CARTESIAN_POINT ( 'NONE',  ( 22.31825301297700648, 1.237144038376295274, 11.49999999999998934 ) ) ;
#68166=ORIENTED_EDGE ( 'NONE', *, *, #93050, .F. ) ;
#68167=CARTESIAN_POINT ( 'NONE',  ( -94.52287095715006160, -23.96127896941631974, -0.6493128931037982499 ) ) ;
#68170=CARTESIAN_POINT ( 'NONE',  ( 6.973883220674568229, 19.69035807221911938, -1.500000000000002220 ) ) ;
#68174=ORIENTED_EDGE ( 'NONE', *, *, #67768, .F. ) ;
#68175=AXIS2_PLACEMENT_3D ( 'NONE', #60738, #21640, #22142 ) ;
#68176=ADVANCED_FACE ( 'NONE', ( #94826 ), #3665, .T. ) ;
#68177=CARTESIAN_POINT ( 'NONE',  ( -51.28881298620314766, -25.27220106976723457, 4.100648920822429488 ) ) ;
#68178=CARTESIAN_POINT ( 'NONE',  ( 10.59196434753715010, 18.29633683537252509, -1.500000000000002220 ) ) ;
#68180=CARTESIAN_POINT ( 'NONE',  ( -117.5170265704868200, -24.51314013834316086, 0.6176544820404215042 ) ) ;
#68181=CARTESIAN_POINT ( 'NONE',  ( -99.87501341000351829, -25.12215651587715115, 6.992709577391502229 ) ) ;
#68182=CARTESIAN_POINT ( 'NONE',  ( -5.167225684058948332, 21.16526716281445530, -1.500000000000002220 ) ) ;
#68183=CARTESIAN_POINT ( 'NONE',  ( -114.5228709571500616, -23.47596703998600631, 11.44779298504228038 ) ) ;
#68184=CARTESIAN_POINT ( 'NONE',  ( -76.64296881555020491, -23.73791477778911840, 11.05961554403170766 ) ) ;
#68185=CARTESIAN_POINT ( 'NONE',  ( -79.78390267227787547, -25.17112743842814027, 6.874869416038779768 ) ) ;
#68186=CARTESIAN_POINT ( 'NONE',  ( -1.994712787082457472, 21.64621699974126656, -1.500000000000002220 ) ) ;
#68188=CARTESIAN_POINT ( 'NONE',  ( 9.556255610625576935, 20.19728179944524271, 11.49999999999999645 ) ) ;
#68189=ORIENTED_EDGE ( 'NONE', *, *, #20181, .T. ) ;
#68190=CARTESIAN_POINT ( 'NONE',  ( -116.5895376238167387, -23.47593901973091235, -1.443836447538997536 ) ) ;
#68192=CARTESIAN_POINT ( 'NONE',  ( -31.52287095715006160, -24.64898659630367206, 1.056161002820817485 ) ) ;
#68193=ORIENTED_EDGE ( 'NONE', *, *, #78882, .F. ) ;
#68197=CARTESIAN_POINT ( 'NONE',  ( -9.361133326760958440, -19.03884994183470880, 11.49999999999998934 ) ) ;
#68199=CARTESIAN_POINT ( 'NONE',  ( -95.62287095715004170, -23.84081130438200802, 10.88220057463249013 ) ) ;
#68200=B_SPLINE_CURVE_WITH_KNOTS ( 'NONE', 3,
 ( #35246, #66216, #88531, #57594, #49483, #97136 ),
 .UNSPECIFIED., .F., .F.,
 ( 4, 2, 4 ),
 ( 6.391158118958419274E-06, 0.001387004593080778557, 0.002767618028042598960 ),
 .UNSPECIFIED. ) ;
#68204=CARTESIAN_POINT ( 'NONE',  ( -18.23339674026497903, -6.527145932826366348, 11.49999999999998934 ) ) ;
#68205=LINE ( 'NONE', #12405, #39207 ) ;
#68206=ORIENTED_EDGE ( 'NONE', *, *, #7723, .T. ) ;
#68207=CARTESIAN_POINT ( 'NONE',  ( -19.39930850525863804, 0.8904154686948315689, 11.49999999999999645 ) ) ;
#68209=EDGE_CURVE ( 'NONE', #77123, #86024, #42061, .T. ) ;
#68213=EDGE_CURVE ( 'NONE', #65697, #33349, #34434, .T. ) ;
#68215=ADVANCED_FACE ( 'NONE', ( #86713 ), #48168, .F. ) ;
#68217=CARTESIAN_POINT ( 'NONE',  ( 0.6594449095415070294, 19.62168050102039629, 11.49999999999998934 ) ) ;
#68218=CARTESIAN_POINT ( 'NONE',  ( -33.62287095715005592, -29.50250243563736774, 8.947779886222150481 ) ) ;
#68219=ORIENTED_EDGE ( 'NONE', *, *, #89960, .T. ) ;
#68221=CARTESIAN_POINT ( 'NONE',  ( 5.689979955356517571, -20.79666814084963278, 11.49999999999998934 ) ) ;
#68222=CARTESIAN_POINT ( 'NONE',  ( -33.58672562287462426, -24.35071581493542325, 9.817618358456039473 ) ) ;
#68223=CARTESIAN_POINT ( 'NONE',  ( -116.5228709571501042, -23.47593901973090524, -1.443836447538996426 ) ) ;
#68224=CARTESIAN_POINT ( 'NONE',  ( -62.62287095715004881, -24.64965695001468404, 8.947790433994185832 ) ) ;
#68225=CARTESIAN_POINT ( 'NONE',  ( -99.59031406714542811, -25.27473316629503941, 3.731155320732701952 ) ) ;
#68226=CARTESIAN_POINT ( 'NONE',  ( -14.58522200957802184, -17.87834940746265389, -1.500000000000002220 ) ) ;
#68228=CARTESIAN_POINT ( 'NONE',  ( -93.51534127454544887, -23.96119346886881019, -0.6495511937832080251 ) ) ;
#68229=CARTESIAN_POINT ( 'NONE',  ( -51.30640140532707960, -25.30285855287542773, 4.744951912546983230 ) ) ;
#68230=CARTESIAN_POINT ( 'NONE',  ( 14.24339680280927567, 14.23919408161895284, 11.49999999999999645 ) ) ;
#68231=CARTESIAN_POINT ( 'NONE',  ( -45.62287095715006302, -24.62285846362216191, 9.038163152653527987 ) ) ;
#68236=CARTESIAN_POINT ( 'NONE',  ( 0.1862606309321278575, -19.90735222434816976, -1.500000000000002220 ) ) ;
#68238=CARTESIAN_POINT ( 'NONE',  ( -68.62287095715005592, -23.47593901973091235, -1.443836447539006196 ) ) ;
#68239=CARTESIAN_POINT ( 'NONE',  ( -11.78406182805296254, 15.88391379356440503, -1.500000000000002220 ) ) ;
#68240=CARTESIAN_POINT ( 'NONE',  ( -126.5893510134409325, -24.51419770103158413, 9.386484678747162747 ) ) ;
#68243=CARTESIAN_POINT ( 'NONE',  ( -37.52287095715008292, -23.73907113217657994, -1.053371485781499306 ) ) ;
#68244=CARTESIAN_POINT ( 'NONE',  ( 16.32338804990218151, -12.73490195939593406, 11.49999999999999645 ) ) ;
#68245=LINE ( 'NONE', #75341, #35404 ) ;
#68247=CARTESIAN_POINT ( 'NONE',  ( -108.5228709571500616, -29.50247984919015209, -1.443849546365048253 ) ) ;
#68248=CARTESIAN_POINT ( 'NONE',  ( -35.58953762381672448, -23.47596703998600276, 11.44779298504227505 ) ) ;
#68249=CARTESIAN_POINT ( 'NONE',  ( 7.533951754900199305, 21.46025436219600024, 11.49999999999999645 ) ) ;
#68251=CARTESIAN_POINT ( 'NONE',  ( -91.62287095715004170, -23.94994826722565762, -0.6494450866342749151 ) ) ;
#68252=EDGE_CURVE ( 'NONE', #51004, #72503, #80358, .T. ) ;
#68254=CARTESIAN_POINT ( 'NONE',  ( 13.23653054071972512, 15.24542462990338088, 11.49999999999998934 ) ) ;
#68257=CARTESIAN_POINT ( 'NONE',  ( -41.46446907970767626, -25.28258282913159860, 4.252216095719075994 ) ) ;
#68258=EDGE_LOOP ( 'NONE', ( #2773, #68595, #29871, #62541 ) ) ;
#68260=ORIENTED_EDGE ( 'NONE', *, *, #36053, .T. ) ;
#68261=DIRECTION ( 'NONE',  ( 0.000000000000000000, 2.173523156925980399E-06, -0.9999999999976378895 ) ) ;
#68262=CARTESIAN_POINT ( 'NONE',  ( 15.42672287639063100, 16.92133821996916865, -1.500000000000002220 ) ) ;
#68263=CARTESIAN_POINT ( 'NONE',  ( -111.3776484685884185, -25.28710546256126079, 4.332404433089555695 ) ) ;
#68264=ADVANCED_FACE ( 'NONE', ( #73492 ), #89720, .T. ) ;
#68265=CARTESIAN_POINT ( 'NONE',  ( 20.55956107658784404, -6.795330137259728787, -1.500000000000002220 ) ) ;
#68266=DIRECTION ( 'NONE',  ( 1.000000000000000000, 3.773278334444167608E-23, 8.201307833595939069E-29 ) ) ;
#68267=CARTESIAN_POINT ( 'NONE',  ( -127.5892766125946451, -24.66019654487200441, 8.947790411086106843 ) ) ;
#68268=CARTESIAN_POINT ( 'NONE',  ( 17.92008016455634589, 10.74458801173053324, 11.49999999999999645 ) ) ;
#68269=VERTEX_POINT ( 'NONE', #81102 ) ;
#68270=PLANE ( 'NONE',  #99949 ) ;
#68271=CARTESIAN_POINT ( 'NONE',  ( -15.01370250125036421, 16.05796621403891677, 11.49999999999998934 ) ) ;
#68272=CARTESIAN_POINT ( 'NONE',  ( -105.5461398891562936, -25.00182538069147142, 7.747789668545045139 ) ) ;
#68273=CARTESIAN_POINT ( 'NONE',  ( -40.50110916354886825, -25.29087034907446707, 2.834725585562781092 ) ) ;
#68275=DIRECTION ( 'NONE',  ( 3.773278334444166432E-23, -1.000000000000000000, 0.000000000000000000 ) ) ;
#68278=CARTESIAN_POINT ( 'NONE',  ( -72.63498091499847931, -24.15620529776628089, 10.23563542870660825 ) ) ;
#68280=B_SPLINE_CURVE_WITH_KNOTS ( 'NONE', 3,
 ( #57517, #87952, #71228, #17936, #11325, #95057 ),
 .UNSPECIFIED., .F., .F.,
 ( 4, 2, 4 ),
 ( 0.000000000000000000, 0.001381645775336347781, 0.002763291550672695562 ),
 .UNSPECIFIED. ) ;
#68282=LINE ( 'NONE', #61183, #30706 ) ;
#68283=DIRECTION ( 'NONE',  ( -3.773278334453079030E-23, 0.9999999999976377785, 2.173523156925979128E-06 ) ) ;
#68284=CARTESIAN_POINT ( 'NONE',  ( -57.64982222934394684, -23.73766607897670866, -1.055555164236458454 ) ) ;
#68285=CARTESIAN_POINT ( 'NONE',  ( -12.12210191164509965, 16.44476101713275185, -1.500000000000002220 ) ) ;
#68286=ORIENTED_EDGE ( 'NONE', *, *, #34481, .T. ) ;
#68288=CARTESIAN_POINT ( 'NONE',  ( -92.52287095715007581, -24.51387760970725083, 9.387446482453409402 ) ) ;
#68291=VERTEX_POINT ( 'NONE', #11583 ) ;
#68292=CARTESIAN_POINT ( 'NONE',  ( -30.47287095715007510, -23.47596699454220470, 11.42688508591989560 ) ) ;
#68293=CARTESIAN_POINT ( 'NONE',  ( -29.54485641382474626, -24.63645763816374412, 6.867484160806894167 ) ) ;
#68294=CARTESIAN_POINT ( 'NONE',  ( 13.57807927624399902, 15.74560944506941951, -1.500000000000002220 ) ) ;
#68296=ORIENTED_EDGE ( 'NONE', *, *, #28043, .F. ) ;
#68297=B_SPLINE_CURVE_WITH_KNOTS ( 'NONE', 3,
 ( #71323, #64740, #19019, #57110 ),
 .UNSPECIFIED., .F., .F.,
 ( 4, 4 ),
 ( 0.000000000000000000, 9.999999999998897304E-05 ),
 .UNSPECIFIED. ) ;
#68298=CARTESIAN_POINT ( 'NONE',  ( -54.62287095715004170, -23.94994826722515668, -0.6494450866351753060 ) ) ;
#68299=ORIENTED_EDGE ( 'NONE', *, *, #54590, .F. ) ;
#68300=CARTESIAN_POINT ( 'NONE',  ( -89.81226385320383088, -25.23397913219354649, 6.409327625488847602 ) ) ;
#68302=EDGE_LOOP ( 'NONE', ( #51657, #6740, #54986, #38441 ) ) ;
#68304=DIRECTION ( 'NONE',  ( -3.773278334453079030E-23, 0.9999999999976377785, 2.173523156925979128E-06 ) ) ;
#68305=FACE_OUTER_BOUND ( 'NONE', #38571, .T. ) ;
#68306=DIRECTION ( 'NONE',  ( -3.773278334453079030E-23, 0.9999999999976377785, 2.173523156925979128E-06 ) ) ;
#68307=B_SPLINE_CURVE_WITH_KNOTS ( 'NONE', 3,
 ( #71685, #32105, #33114, #2678, #23989, #95010 ),
 .UNSPECIFIED., .F., .F.,
 ( 4, 2, 4 ),
 ( 0.000000000000000000, 0.001380764517854767568, 0.002761529035709535135 ),
 .UNSPECIFIED. ) ;
#68308=CARTESIAN_POINT ( 'NONE',  ( -92.51226550044627572, -24.15620529776627734, 10.23563542870659937 ) ) ;
#68310=CARTESIAN_POINT ( 'NONE',  ( 17.13038851031509680, -14.05419017248541813, 11.49999999999999645 ) ) ;
#68312=CARTESIAN_POINT ( 'NONE',  ( -108.5505322218205464, -24.51314013834316086, 0.6176544820404235026 ) ) ;
#68313=CARTESIAN_POINT ( 'NONE',  ( -18.78231125015805958, 12.62931641965373153, -1.500000000000002220 ) ) ;
#68314=CARTESIAN_POINT ( 'NONE',  ( -87.55620429048337883, -23.47593901973091235, -1.443836447539002865 ) ) ;
#68320=EDGE_CURVE ( 'NONE', #22811, #80400, #27317, .T. ) ;
#68321=CARTESIAN_POINT ( 'NONE',  ( 0.3675393366473880818, 20.13074986235200470, 11.49999999999998934 ) ) ;
#68323=VERTEX_POINT ( 'NONE', #4976 ) ;
#68325=CARTESIAN_POINT ( 'NONE',  ( -103.5562042904833930, -24.64965694238575011, 8.947790433994194714 ) ) ;
#68326=CARTESIAN_POINT ( 'NONE',  ( -22.22805510923732086, 2.117028069546627922, -1.500000000000002220 ) ) ;
#68328=VERTEX_POINT ( 'NONE', #13573 ) ;
#68330=CARTESIAN_POINT ( 'NONE',  ( -76.52287095715007581, -24.64965694238408034, 8.947790433994198267 ) ) ;
#68331=CARTESIAN_POINT ( 'NONE',  ( -80.85315749703953259, -25.04053079579781382, 7.527282393074037792 ) ) ;
#68333=EDGE_CURVE ( 'NONE', #47870, #6498, #93643, .T. ) ;
#68334=CARTESIAN_POINT ( 'NONE',  ( -102.5562042904834072, -23.47593901973091235, -1.443836447539001089 ) ) ;
#68335=ADVANCED_FACE ( 'NONE', ( #98813 ), #23177, .T. ) ;
#68337=CARTESIAN_POINT ( 'NONE',  ( 6.866622826037362515, -18.30913693658520103, 11.49999999999998934 ) ) ;
#68339=EDGE_CURVE ( 'NONE', #50965, #26504, #70095, .T. ) ;
#68340=CARTESIAN_POINT ( 'NONE',  ( -2.231587876719630437, -21.34735720706076378, 11.49999999999998934 ) ) ;
#68343=CARTESIAN_POINT ( 'NONE',  ( -115.5562042904833930, -24.99132157543166954, 2.256160258750668834 ) ) ;
#68344=CARTESIAN_POINT ( 'NONE',  ( -7.509321099650855480, 21.62252279970214985, -1.500000000000002220 ) ) ;
#68345=AXIS2_PLACEMENT_3D ( 'NONE', #35986, #51219, #66959 ) ;
#68347=CARTESIAN_POINT ( 'NONE',  ( -106.5159469206628842, -24.15620529776629510, 10.23563542870659582 ) ) ;
#68349=CARTESIAN_POINT ( 'NONE',  ( -0.003041637939312698616, 19.98351707251910980, 11.49999999999999645 ) ) ;
#68350=CARTESIAN_POINT ( 'NONE',  ( -50.52287095715006870, -24.52232992886363405, 0.6492154411905944889 ) ) ;
#68351=CARTESIAN_POINT ( 'NONE',  ( -74.64913626771259203, -23.48786465467241058, 11.44779295918254824 ) ) ;
#68353=ORIENTED_EDGE ( 'NONE', *, *, #63224, .T. ) ;
#68354=CARTESIAN_POINT ( 'NONE',  ( -89.52287095715006160, -24.64898659630528854, 1.056161002820827921 ) ) ;
#68357=CARTESIAN_POINT ( 'NONE',  ( 6.244050601037331560, 20.82503750550150912, 11.49999999999998934 ) ) ;
#68359=CARTESIAN_POINT ( 'NONE',  ( 17.47348308817029405, 8.859467055162037141, -1.500000000000002220 ) ) ;
#68360=CARTESIAN_POINT ( 'NONE',  ( -99.29687923781919778, -25.26138073939643292, 6.149712181314777482 ) ) ;
#68361=EDGE_CURVE ( 'NONE', #36016, #45083, #35061, .T. ) ;
#68364=CARTESIAN_POINT ( 'NONE',  ( -108.8968792378192632, -25.08859304705472937, 7.294522420277893993 ) ) ;
#68366=CARTESIAN_POINT ( 'NONE',  ( 20.06376955418885899, 4.186446014007643157, 11.49999999999999645 ) ) ;
#68367=CARTESIAN_POINT ( 'NONE',  ( -59.52287095715006160, -23.48786465467241769, 11.44779295918254824 ) ) ;
#68371=ORIENTED_EDGE ( 'NONE', *, *, #15865, .F. ) ;
#68374=CARTESIAN_POINT ( 'NONE',  ( -101.5562042904833788, -23.48783264082478439, -1.443836473390061936 ) ) ;
#68375=CARTESIAN_POINT ( 'NONE',  ( -123.5228709571499763, -23.95044443724992789, 10.65354141964648527 ) ) ;
#68377=CARTESIAN_POINT ( 'NONE',  ( -42.62287095715004170, -24.33927499327853994, 9.819080762295818943 ) ) ;
#68380=CARTESIAN_POINT ( 'NONE',  ( 23.03040035405544472, 1.057182387018521963, 11.49999999999999645 ) ) ;
#68381=CARTESIAN_POINT ( 'NONE',  ( 12.37853024107498534, -19.16169124346054176, 11.49999999999998934 ) ) ;
#68382=CARTESIAN_POINT ( 'NONE',  ( -70.27422298781921484, -25.30458796900497376, 4.851635164322918747 ) ) ;
#68387=CARTESIAN_POINT ( 'NONE',  ( -110.5169900288274647, -24.15503026093914229, -0.2815557561904443729 ) ) ;
#68389=CARTESIAN_POINT ( 'NONE',  ( -12.72821696145241255, -17.84489267850806726, 11.49999999999998934 ) ) ;
#68390=CARTESIAN_POINT ( 'NONE',  ( -87.58953762381671027, -24.65952944569304961, 1.056160979905701458 ) ) ;
#68391=CARTESIAN_POINT ( 'NONE',  ( -87.62358879123520694, -24.66019654487200441, 8.947790411086112172 ) ) ;
#68393=CARTESIAN_POINT ( 'NONE',  ( -78.63379020606802783, -24.15543982623907127, -0.2315651400026641771 ) ) ;
#68394=FACE_OUTER_BOUND ( 'NONE', #89836, .T. ) ;
#68395=CARTESIAN_POINT ( 'NONE',  ( -122.6228709571500133, -24.51387760970724017, 9.387446482453405849 ) ) ;
#68397=CARTESIAN_POINT ( 'NONE',  ( 0.3735783541106268979, -20.45636175344465713, -1.500000000000002220 ) ) ;
#68398=VERTEX_POINT ( 'NONE', #15573 ) ;
#68400=ORIENTED_EDGE ( 'NONE', *, *, #99248, .T. ) ;
#68401=ORIENTED_EDGE ( 'NONE', *, *, #80061, .F. ) ;
#68402=CARTESIAN_POINT ( 'NONE',  ( 22.88022663504679599, 2.825535151426334934, 11.49999999999998934 ) ) ;
#68403=CARTESIAN_POINT ( 'NONE',  ( -61.57930669521469724, -24.65952944569304961, 1.056160979905699682 ) ) ;
#68404=CARTESIAN_POINT ( 'NONE',  ( 14.48468284575590204, 14.13777120147990729, -1.500000000000002220 ) ) ;
#68406=CARTESIAN_POINT ( 'NONE',  ( -29.26978116671819663, -25.09101794427064291, 3.118813907533751983 ) ) ;
#68407=CARTESIAN_POINT ( 'NONE',  ( -41.86995616089614458, -25.28979658489737048, 4.210709715701590028 ) ) ;
#68408=CARTESIAN_POINT ( 'NONE',  ( -49.62287095715005592, -29.50248528299804818, 1.056150453629033370 ) ) ;
#68409=FACE_OUTER_BOUND ( 'NONE', #2171, .T. ) ;
#68410=CARTESIAN_POINT ( 'NONE',  ( -9.048234560742015375, 19.43086790383670603, 11.49999999999999645 ) ) ;
#68412=DIRECTION ( 'NONE',  ( 0.000000000000000000, 0.9999999999976377785, 2.173523156925979128E-06 ) ) ;
#68413=CARTESIAN_POINT ( 'NONE',  ( -34.62287095715005592, -23.72747288104469732, -1.053458166803227902 ) ) ;
#68414=EDGE_LOOP ( 'NONE', ( #29231, #72677, #12399, #70169 ) ) ;
#68415=CARTESIAN_POINT ( 'NONE',  ( -20.39401028033356766, -3.670942005906183692, 11.49999999999998934 ) ) ;
#68419=B_SPLINE_SURFACE_WITH_KNOTS ( 'NONE', 3, 3, ( 
 ( #40015, #10066, #55759, #1968 ),
 ( #55258, #41027, #32910, #62880 ),
 ( #46641, #79068, #54756, #16172 ),
 ( #93288, #62362, #25789, #47641 ),
 ( #71980, #15674, #16671, #78557 ),
 ( #23783, #95304, #85691, #77559 ),
 ( #69963, #24779, #86686, #32407 ) ),
 .UNSPECIFIED., .F., .F., .F.,
 ( 4, 3, 4 ),
 ( 4, 4 ),
 ( 0.7945040050992232539, 0.8970133687736493444, 0.9995227324480754350 ),
 ( 0.06951166112253108487, 0.07055647687300854731 ),
 .UNSPECIFIED. ) ;
#68420=B_SPLINE_CURVE_WITH_KNOTS ( 'NONE', 3,
 ( #59708, #91135, #52086, #74903 ),
 .UNSPECIFIED., .F., .F.,
 ( 4, 4 ),
 ( 0.000000000000000000, 9.999999999999592548E-05 ),
 .UNSPECIFIED. ) ;
#68421=CARTESIAN_POINT ( 'NONE',  ( -91.52287095715010423, -24.35013146730204525, 9.818937971375097717 ) ) ;
#68424=ORIENTED_EDGE ( 'NONE', *, *, #7544, .F. ) ;
#68425=CARTESIAN_POINT ( 'NONE',  ( 14.12621959167996977, 16.79361087625908056, 11.49999999999999645 ) ) ;
#68426=CARTESIAN_POINT ( 'NONE',  ( -37.55288945954268343, -23.96169478059712432, 10.65365249895718591 ) ) ;
#68427=CARTESIAN_POINT ( 'NONE',  ( 11.36372850657041589, -19.49111573544105624, 11.49999999999998934 ) ) ;
#68428=CARTESIAN_POINT ( 'NONE',  ( -20.02981537788295441, -6.213780249082809348, 11.49999999999998934 ) ) ;
#68429=CARTESIAN_POINT ( 'NONE',  ( -109.4421867512570401, -25.31228852508138516, 5.310510576710047559 ) ) ;
#68431=VERTEX_POINT ( 'NONE', #60773 ) ;
#68432=AXIS2_PLACEMENT_3D ( 'NONE', #92312, #20795, #22286 ) ;
#68433=ORIENTED_EDGE ( 'NONE', *, *, #88185, .T. ) ;
#68434=VERTEX_POINT ( 'NONE', #77464 ) ;
#68436=CARTESIAN_POINT ( 'NONE',  ( -66.62727618262151452, -24.51314013834316441, 0.6176544820404136216 ) ) ;
#68437=CARTESIAN_POINT ( 'NONE',  ( -2.508422780830330989, 21.39056295969660582, -1.500000000000002220 ) ) ;
#68439=ORIENTED_EDGE ( 'NONE', *, *, #52057, .T. ) ;
#68440=CARTESIAN_POINT ( 'NONE',  ( -20.28541985502614509, -5.886007371444655689, -1.500000000000002220 ) ) ;
#68442=ADVANCED_FACE ( 'NONE', ( #7965 ), #38919, .T. ) ;
#68445=CARTESIAN_POINT ( 'NONE',  ( -99.29687923781919778, -25.25133594952260552, 6.149712203147405631 ) ) ;
#68447=CARTESIAN_POINT ( 'NONE',  ( 4.265775719338400052, 21.77767432286298543, -1.500000000000002220 ) ) ;
#68449=CARTESIAN_POINT ( 'NONE',  ( -71.50229426790137666, -24.34968618360933945, 0.1864209137778822800 ) ) ;
#68452=CARTESIAN_POINT ( 'NONE',  ( -108.9857387129618758, -25.29479647189234015, 4.484512479850331523 ) ) ;
#68453=FACE_OUTER_BOUND ( 'NONE', #98628, .T. ) ;
#68454=CARTESIAN_POINT ( 'NONE',  ( -41.86995616089613748, -25.31624451996179914, 4.210709658216391205 ) ) ;
#68458=CARTESIAN_POINT ( 'NONE',  ( -15.63568348323273227, -11.59263941501104966, 11.49999999999998934 ) ) ;
#68460=CARTESIAN_POINT ( 'NONE',  ( -15.06583839362908961, -15.15408912208086534, 11.49999999999998934 ) ) ;
#68461=CARTESIAN_POINT ( 'NONE',  ( -62.51546559041052120, -23.73766607897669445, -1.055555164236454901 ) ) ;
#68462=CARTESIAN_POINT ( 'NONE',  ( -90.25664208330698557, -25.26877915520014639, 5.947789088310639904 ) ) ;
#68463=CARTESIAN_POINT ( 'NONE',  ( -79.62287095715007013, -23.96127896941631619, -0.6493128931037847051 ) ) ;
#68465=CARTESIAN_POINT ( 'NONE',  ( 19.70651319644445465, -11.07993823016455792, -1.500000000000002220 ) ) ;
#68466=B_SPLINE_CURVE_WITH_KNOTS ( 'NONE', 3,
 ( #38942, #24217, #382, #31330, #62299, #54683, #85614, #55192, #16103, #47072, #70400, #78494, #11001, #27231 ),
 .UNSPECIFIED., .F., .F.,
 ( 4, 2, 2, 2, 2, 2, 4 ),
 ( 0.000000000000000000, 0.0002390712444983297737, 0.0004781424889966595475, 0.0009562849779933203960, 0.001434427466989981245, 0.001673498711488311669, 0.001912569955986642093 ),
 .UNSPECIFIED. ) ;
#68468=ORIENTED_EDGE ( 'NONE', *, *, #12569, .F. ) ;
#68469=CARTESIAN_POINT ( 'NONE',  ( -39.52287095715006870, -29.50247984919015209, -1.443849546365060466 ) ) ;
#68470=CARTESIAN_POINT ( 'NONE',  ( -57.62287095715004881, -24.66019654487199020, 8.947790411086131712 ) ) ;
#68471=CARTESIAN_POINT ( 'NONE',  ( 16.01007288495529224, -11.65062672332236104, 11.49999999999999645 ) ) ;
#68476=LINE ( 'NONE', #99409, #14179 ) ;
#68477=CARTESIAN_POINT ( 'NONE',  ( 1.064956243273112557, 21.61254047163424019, 11.49999999999998934 ) ) ;
#68478=CARTESIAN_POINT ( 'NONE',  ( -27.60906388276667656, -24.79421432578786977, 7.602479806744845803 ) ) ;
#68479=CARTESIAN_POINT ( 'NONE',  ( 18.22972481837485859, -6.773019484731225504, -1.500000000000002220 ) ) ;
#68480=CARTESIAN_POINT ( 'NONE',  ( -129.6228709571500133, -24.51387760970727214, 9.387446482453416507 ) ) ;
#68482=CARTESIAN_POINT ( 'NONE',  ( 12.93213199337649044, -14.99640713134888692, -1.500000000000002220 ) ) ;
#68484=CARTESIAN_POINT ( 'NONE',  ( 15.76184642470745700, 12.85868457875834103, 11.49999999999999645 ) ) ;
#68485=CARTESIAN_POINT ( 'NONE',  ( -80.52209458990078872, -23.48783264082477018, -1.443836473390096131 ) ) ;
#68488=ORIENTED_EDGE ( 'NONE', *, *, #12535, .T. ) ;
#68489=CARTESIAN_POINT ( 'NONE',  ( -0.04073145180001176008, -22.52269934801777040, 8.549170486301877148 ) ) ;
#68490=LINE ( 'NONE', #29417, #96299 ) ;
#68492=CARTESIAN_POINT ( 'NONE',  ( -82.55620429048337883, -23.48786465467241058, 11.44779295918255180 ) ) ;
#68493=CARTESIAN_POINT ( 'NONE',  ( -50.74135369471817825, -25.12871364012075048, 7.068779736917301548 ) ) ;
#68494=CARTESIAN_POINT ( 'NONE',  ( -19.74138705131307248, -3.616033589355840849, -1.500000000000002220 ) ) ;
#68495=B_SPLINE_CURVE_WITH_KNOTS ( 'NONE', 3,
 ( #66523, #58886, #26933, #20297, #97440, #49788 ),
 .UNSPECIFIED., .F., .F.,
 ( 4, 2, 4 ),
 ( 6.391158118952235087E-06, 0.001387004593080775738, 0.002767618028042598960 ),
 .UNSPECIFIED. ) ;
#68498=CARTESIAN_POINT ( 'NONE',  ( -63.95380932530888884, -23.56000036390796382, 11.50199999999999889 ) ) ;
#68499=ADVANCED_FACE ( 'NONE', ( #71383 ), #39919, .F. ) ;
#68500=CARTESIAN_POINT ( 'NONE',  ( -7.509321099650855480, 21.62252279970214985, 11.49999999999999645 ) ) ;
#68501=CARTESIAN_POINT ( 'NONE',  ( -49.84984290111637506, -25.31297183315718158, 4.578679947858303123 ) ) ;
#68503=DIRECTION ( 'NONE',  ( -3.773278334453079030E-23, 0.9999999999976377785, 2.173523156925979128E-06 ) ) ;
#68508=EDGE_CURVE ( 'NONE', #94949, #46688, #94353, .T. ) ;
#68509=PLANE ( 'NONE',  #71220 ) ;
#68510=ORIENTED_EDGE ( 'NONE', *, *, #39914, .T. ) ;
#68511=CARTESIAN_POINT ( 'NONE',  ( 3.729398819442638846, -20.01364129133569136, -1.500000000000002220 ) ) ;
#68513=CARTESIAN_POINT ( 'NONE',  ( -8.204236019480731557, -21.45505762417899831, 11.49999999999998934 ) ) ;
#68514=DIRECTION ( 'NONE',  ( 0.000000000000000000, 2.173523156925980399E-06, -0.9999999999976378895 ) ) ;
#68516=CARTESIAN_POINT ( 'NONE',  ( -101.2400011396082817, -25.16928559910140706, 6.818282878674360781 ) ) ;
#68517=CARTESIAN_POINT ( 'NONE',  ( -116.5228709571500474, -23.73934037231757443, 11.05740245334327909 ) ) ;
#68520=CARTESIAN_POINT ( 'NONE',  ( -96.62287095715009855, -23.94994826722515668, -0.6494450866351711982 ) ) ;
#68521=CARTESIAN_POINT ( 'NONE',  ( -21.26230640008892792, -0.7210608269398429693, 11.49999999999999645 ) ) ;
#68522=ORIENTED_EDGE ( 'NONE', *, *, #24806, .F. ) ;
#68524=VERTEX_POINT ( 'NONE', #32306 ) ;
#68525=CARTESIAN_POINT ( 'NONE',  ( 21.60277357391871433, -5.133695162202882578, 11.49999999999998934 ) ) ;
#68526=CARTESIAN_POINT ( 'NONE',  ( -9.109090448966927767, 18.51201596650851400, -1.500000000000002220 ) ) ;
#68527=ORIENTED_EDGE ( 'NONE', *, *, #78638, .F. ) ;
#68528=VECTOR ( 'NONE', #42171, 1000.000000000000227 ) ;
#68529=ORIENTED_EDGE ( 'NONE', *, *, #35979, .T. ) ;
#68533=ORIENTED_EDGE ( 'NONE', *, *, #60214, .T. ) ;
#68537=CARTESIAN_POINT ( 'NONE',  ( 18.58881047053902691, 9.431966241625852732, -1.500000000000002220 ) ) ;
#68538=CARTESIAN_POINT ( 'NONE',  ( -6.457742198559264679, -20.83860622980983024, 11.49999999999999645 ) ) ;
#68539=CARTESIAN_POINT ( 'NONE',  ( -40.45231480346743069, -25.31583771044696718, 5.081397513335677907 ) ) ;
#68541=CARTESIAN_POINT ( 'NONE',  ( 22.31695869535024102, -2.478243017838637652, -1.500000000000002220 ) ) ;
#68542=CARTESIAN_POINT ( 'NONE',  ( -50.72939492065860634, -25.26334739434139820, 4.679804835100300764 ) ) ;
#68543=EDGE_CURVE ( 'NONE', #20514, #31325, #57169, .T. ) ;
#68544=ORIENTED_EDGE ( 'NONE', *, *, #42918, .T. ) ;
#68547=B_SPLINE_SURFACE_WITH_KNOTS ( 'NONE', 3, 3, ( 
 ( #65993, #96910, #13156, #89799 ),
 ( #97892, #27405, #4574, #65493 ),
 ( #90295, #81690, #96414, #18777 ),
 ( #49759, #12163, #35523, #81185 ),
 ( #80686, #59347, #73580, #43131 ),
 ( #58364, #42148, #26404, #28388 ),
 ( #74567, #12665, #89302, #74082 ) ),
 .UNSPECIFIED., .F., .F., .F.,
 ( 4, 3, 4 ),
 ( 4, 4 ),
 ( 0.3389043340504379054, 0.5146335846998002506, 0.6903628353491626513 ),
 ( 0.7862494037672983493, 0.8171928712212183088 ),
 .UNSPECIFIED. ) ;
#68548=VERTEX_POINT ( 'NONE', #18575 ) ;
#68552=CARTESIAN_POINT ( 'NONE',  ( -21.31669061289120037, -0.5855882196083471714, -1.500000000000002220 ) ) ;
#68553=ORIENTED_EDGE ( 'NONE', *, *, #73823, .T. ) ;
#68555=CARTESIAN_POINT ( 'NONE',  ( -17.04133944854041616, 12.32129857345222845, 11.49999999999998934 ) ) ;
#68556=CARTESIAN_POINT ( 'NONE',  ( -30.48449779480992561, -24.66625093156569903, 1.095666116063856776 ) ) ;
#68557=EDGE_CURVE ( 'NONE', #91720, #91650, #86592, .T. ) ;
#68558=B_SPLINE_CURVE_WITH_KNOTS ( 'NONE', 3,
 ( #44833, #67182, #37704, #61058, #60065, #6255 ),
 .UNSPECIFIED., .F., .F.,
 ( 4, 2, 4 ),
 ( 6.391158118952235087E-06, 0.001387004593080777906, 0.002767618028042603297 ),
 .UNSPECIFIED. ) ;
#68559=CARTESIAN_POINT ( 'NONE',  ( -113.5228709571500474, -24.50321055353803601, 9.387540953477508054 ) ) ;
#68560=B_SPLINE_CURVE_WITH_KNOTS ( 'NONE', 3,
 ( #11722, #82733, #58425, #81743, #58911, #89854 ),
 .UNSPECIFIED., .F., .F.,
 ( 4, 2, 4 ),
 ( 6.391158118970788496E-06, 0.001387004593080791133, 0.002767618028042611537 ),
 .UNSPECIFIED. ) ;
#68562=CARTESIAN_POINT ( 'NONE',  ( 16.65356921002588919, 14.36988287374134821, -1.500000000000002220 ) ) ;
#68563=CARTESIAN_POINT ( 'NONE',  ( -87.63898554099732507, -23.73766607897671221, -1.055555164236430032 ) ) ;
#68564=ORIENTED_EDGE ( 'NONE', *, *, #20896, .F. ) ;
#68565=CARTESIAN_POINT ( 'NONE',  ( -122.5185765871470238, -24.66019654487200086, 8.947790411086110396 ) ) ;
#68566=AXIS2_PLACEMENT_3D ( 'NONE', #5264, #50450, #73292 ) ;
#68567=EDGE_CURVE ( 'NONE', #80888, #84261, #97931, .T. ) ;
#68569=CARTESIAN_POINT ( 'NONE',  ( -84.59927232378923634, -23.73791477778912196, 11.05961554403170588 ) ) ;
#68571=EDGE_CURVE ( 'NONE', #31523, #85746, #51950, .T. ) ;
#68572=CARTESIAN_POINT ( 'NONE',  ( -41.62287095715005592, -23.73907113216990084, -1.053371485793234807 ) ) ;
#68573=LINE ( 'NONE', #29495, #96691 ) ;
#68574=CARTESIAN_POINT ( 'NONE',  ( 10.72677997844354536, -18.41129465587203740, -1.500000000000002220 ) ) ;
#68578=DIRECTION ( 'NONE',  ( -3.773278334453079618E-23, 0.9999999999976377785, 2.173523156925979975E-06 ) ) ;
#68579=DIRECTION ( 'NONE',  ( 0.000000000000000000, -0.9999999999976377785, -2.173523156925979128E-06 ) ) ;
#68580=CARTESIAN_POINT ( 'NONE',  ( -18.83616483605274539, -12.25834331966736102, -1.500000000000002220 ) ) ;
#68581=CARTESIAN_POINT ( 'NONE',  ( -109.9087718796684356, -25.21970293610405633, 6.713732480141158199 ) ) ;
#68582=ORIENTED_EDGE ( 'NONE', *, *, #85269, .T. ) ;
#68583=DIRECTION ( 'NONE',  ( 0.000000000000000000, -0.9999999999976377785, -2.173523156925979128E-06 ) ) ;
#68584=CARTESIAN_POINT ( 'NONE',  ( -19.61951575358169819, -0.1233725505697131491, 11.49999999999999645 ) ) ;
#68585=CARTESIAN_POINT ( 'NONE',  ( -68.62287095715004170, -23.72747288104441665, -1.053458166803662444 ) ) ;
#68587=EDGE_CURVE ( 'NONE', #86142, #75490, #53218, .T. ) ;
#68589=CARTESIAN_POINT ( 'NONE',  ( -69.06683892470179842, -25.29165132073142885, 5.590026102521621354 ) ) ;
#68591=CARTESIAN_POINT ( 'NONE',  ( -124.6234875168763665, -24.66019654487200441, 8.947790411086108620 ) ) ;
#68592=CARTESIAN_POINT ( 'NONE',  ( -25.53604547899276156, -24.92361880405457697, 5.314701426448082522 ) ) ;
#68594=CARTESIAN_POINT ( 'NONE',  ( 3.669390655483735220, -19.36157329643844704, -1.500000000000002220 ) ) ;
#68595=ORIENTED_EDGE ( 'NONE', *, *, #27342, .F. ) ;
#68598=AXIS2_PLACEMENT_3D ( 'NONE', #98641, #59111, #21021 ) ;
#68601=CARTESIAN_POINT ( 'NONE',  ( -109.6228709571500843, -23.96177878511308990, 10.65340807706329684 ) ) ;
#68603=CARTESIAN_POINT ( 'NONE',  ( -55.48559462693079780, -24.73486907724917572, 1.287355809206960355 ) ) ;
#68606=CARTESIAN_POINT ( 'NONE',  ( -31.79944283184905274, -24.86441978397624553, 8.247789967200544581 ) ) ;
#68607=AXIS2_PLACEMENT_3D ( 'NONE', #34521, #72094, #89305 ) ;
#68608=CARTESIAN_POINT ( 'NONE',  ( -107.5222082047791190, -23.48783264082479505, -1.443836473390060826 ) ) ;
#68609=CARTESIAN_POINT ( 'NONE',  ( -19.95764006394758638, 0.7380318605572177004, 11.49999999999998934 ) ) ;
#68610=ADVANCED_FACE ( 'NONE', ( #19075 ), #89593, .T. ) ;
#68611=CARTESIAN_POINT ( 'NONE',  ( -95.55620429048337883, -25.00182538069145721, 7.747789668545099317 ) ) ;
#68612=CARTESIAN_POINT ( 'NONE',  ( -51.45327580174686943, -25.31044044580817243, 4.639198480576497197 ) ) ;
#68613=EDGE_LOOP ( 'NONE', ( #63819, #35211, #97216, #92701 ) ) ;
#68614=EDGE_CURVE ( 'NONE', #33873, #30676, #5929, .T. ) ;
#68615=CARTESIAN_POINT ( 'NONE',  ( -119.5172027492807416, -24.65952944569305672, 1.056160979905715003 ) ) ;
#68616=DIRECTION ( 'NONE',  ( -3.773278334453079030E-23, 0.9999999999976377785, 2.173523156925979128E-06 ) ) ;
#68618=FACE_OUTER_BOUND ( 'NONE', #24027, .T. ) ;
#68619=CARTESIAN_POINT ( 'NONE',  ( -28.27781825664440873, -25.26026305157151697, 1.715749184898614166 ) ) ;
#68621=B_SPLINE_SURFACE_WITH_KNOTS ( 'NONE', 3, 3, ( 
 ( #61063, #53949, #67684, #38201 ),
 ( #69157, #52949, #90996, #52447 ),
 ( #21467, #6259, #37218, #99095 ),
 ( #79264, #1659, #62559, #24481 ),
 ( #17878, #55447, #25987, #55952 ),
 ( #86387, #1156, #16365, #78254 ),
 ( #56459, #56959, #54946, #47831 ),
 ( #8767, #77748, #85886, #8264 ),
 ( #32092, #86882, #39202, #41223 ),
 ( #72176, #47331, #93989, #15862 ) ),
 .UNSPECIFIED., .F., .F., .F.,
 ( 4, 3, 3, 4 ),
 ( 4, 4 ),
 ( 0.7022005934544800487, 0.7765311282028792839, 0.8508616629512784080, 0.9995227324480768782 ),
 ( 0.9496086015441148609, 0.9511872794485528582 ),
 .UNSPECIFIED. ) ;
#68622=CARTESIAN_POINT ( 'NONE',  ( -79.62287095715004170, -23.96177878511308634, 10.65340807706329862 ) ) ;
#68623=ADVANCED_FACE ( 'NONE', ( #11468 ), #42441, .F. ) ;
#68625=VERTEX_POINT ( 'NONE', #96699 ) ;
#68628=CARTESIAN_POINT ( 'NONE',  ( -3.898967980886277829, 19.90457959416237088, 11.49999999999998934 ) ) ;
#68629=CARTESIAN_POINT ( 'NONE',  ( -122.6239442167820215, -24.51314013834316086, 0.6176544820404212821 ) ) ;
#68631=CARTESIAN_POINT ( 'NONE',  ( -117.6228709571500417, -24.65952944569305316, 1.056160979905706121 ) ) ;
#68632=AXIS2_PLACEMENT_3D ( 'NONE', #51710, #36979, #82649 ) ;
#68634=EDGE_LOOP ( 'NONE', ( #12354, #28870, #7780, #14743 ) ) ;
#68637=CARTESIAN_POINT ( 'NONE',  ( -2.706554608146168217, 19.95013100808389339, -1.500000000000002220 ) ) ;
#68638=VECTOR ( 'NONE', #11483, 1000.000000000000114 ) ;
#68639=CARTESIAN_POINT ( 'NONE',  ( 20.24497096899912307, 5.935080660949433096, 11.49999999999999645 ) ) ;
#68640=CARTESIAN_POINT ( 'NONE',  ( -32.52287095715007581, -24.51283580621450398, 0.6167428607045326583 ) ) ;
#68641=CARTESIAN_POINT ( 'NONE',  ( 12.17348956504948987, -18.45705692928949659, -1.500000000000002220 ) ) ;
#68643=CARTESIAN_POINT ( 'NONE',  ( 18.67943556539783856, 8.552475402716291697, -1.500000000000002220 ) ) ;
#68644=DIRECTION ( 'NONE',  ( 1.000000000000000000, 3.773278334444168195E-23, 8.201307811038811694E-29 ) ) ;
#68645=B_SPLINE_CURVE_WITH_KNOTS ( 'NONE', 3,
 ( #80990, #25697, #11473, #48560, #9974, #40928, #71890, #2374, #33305, #10472, #41430, #75856, #91584, #68263 ),
 .UNSPECIFIED., .F., .F.,
 ( 4, 2, 2, 2, 2, 2, 4 ),
 ( 0.000000000000000000, 0.0002036734231732265489, 0.0004073468463464530978, 0.0008146936926928669475, 0.001222040539039280851, 0.001425713962212487532, 0.001629387385385694430 ),
 .UNSPECIFIED. ) ;
#68646=CARTESIAN_POINT ( 'NONE',  ( -126.6228709571500559, -23.47593901973091235, -1.443836447538995760 ) ) ;
#68648=CARTESIAN_POINT ( 'NONE',  ( -70.62287095715005592, -29.50248789122583659, 2.256150453626215580 ) ) ;
#68649=ORIENTED_EDGE ( 'NONE', *, *, #88534, .F. ) ;
#68651=CARTESIAN_POINT ( 'NONE',  ( -72.58953762381673869, -24.64965694238406968, 8.947790433994660120 ) ) ;
#68655=PLANE ( 'NONE',  #61580 ) ;
#68657=DIRECTION ( 'NONE',  ( -0.000000000000000000, 2.173523156925979552E-06, -0.9999999999976378895 ) ) ;
#68658=CARTESIAN_POINT ( 'NONE',  ( -17.42616458466809704, -11.11377323884725321, -1.500000000000002220 ) ) ;
#68659=CARTESIAN_POINT ( 'NONE',  ( 20.55510029441247610, -6.647428040031946317, 11.49999999999999645 ) ) ;
#68662=CARTESIAN_POINT ( 'NONE',  ( -57.62287095715004881, -24.64965695001468404, 8.947790433994185832 ) ) ;
#68663=CARTESIAN_POINT ( 'NONE',  ( -22.37156870845955225, 0.5457896250522937809, -1.500000000000002220 ) ) ;
#68664=CARTESIAN_POINT ( 'NONE',  ( -111.5228709571500616, -23.47596703998600631, 11.44779298504228038 ) ) ;
#68665=CARTESIAN_POINT ( 'NONE',  ( -84.63259839552451069, -24.15543982623907482, -0.2315651400026629836 ) ) ;
#68669=CARTESIAN_POINT ( 'NONE',  ( 2.299058169534009100, 20.76012671103276475, 11.49999999999998934 ) ) ;
#68671=CARTESIAN_POINT ( 'NONE',  ( -67.59731500115069025, -23.96169478059713853, 10.65365249895717881 ) ) ;
#68674=VECTOR ( 'NONE', #89686, 1000.000000000000114 ) ;
#68675=CARTESIAN_POINT ( 'NONE',  ( -109.5890780322650357, -24.35071581493543746, 9.817618358456025263 ) ) ;
#68676=CARTESIAN_POINT ( 'NONE',  ( 9.297385241821217505, 19.04214385377821017, -1.500000000000002220 ) ) ;
#68678=CARTESIAN_POINT ( 'NONE',  ( -117.6242417137320615, -24.51314013834316086, 0.6176544820404201719 ) ) ;
#68680=CARTESIAN_POINT ( 'NONE',  ( -19.96617879207914825, 8.700599545123990808, -1.500000000000002220 ) ) ;
#68682=VECTOR ( 'NONE', #85551, 1000.000000000000114 ) ;
#68684=CARTESIAN_POINT ( 'NONE',  ( -80.52287095715006160, -23.47593901973090169, -1.443836447538996648 ) ) ;
#68685=CARTESIAN_POINT ( 'NONE',  ( 12.24854465327799424, 17.96525243877979605, -1.500000000000002220 ) ) ;
#68686=CARTESIAN_POINT ( 'NONE',  ( -79.01600328727082001, -25.22409940181762167, 6.494944116009313539 ) ) ;
#68687=EDGE_CURVE ( 'NONE', #29538, #18147, #85910, .T. ) ;
#68688=CARTESIAN_POINT ( 'NONE',  ( 17.40631026334068565, 13.93540124644318645, 11.49999999999999645 ) ) ;
#68690=CARTESIAN_POINT ( 'NONE',  ( -40.62287095715005592, -29.50250786944525672, 11.44777988621624232 ) ) ;
#68693=ORIENTED_EDGE ( 'NONE', *, *, #72561, .F. ) ;
#68697=CARTESIAN_POINT ( 'NONE',  ( -126.2228709571500644, -23.47596703998600987, 11.44779298504227860 ) ) ;
#68698=CARTESIAN_POINT ( 'NONE',  ( 19.29917393477590437, 8.764703196630867055, -1.500000000000002220 ) ) ;
#68700=ADVANCED_FACE ( 'NONE', ( #59152 ), #50534, .F. ) ;
#68701=CARTESIAN_POINT ( 'NONE',  ( -79.20032202190461135, -25.03138152274833672, 6.885560112372425934 ) ) ;
#68702=CARTESIAN_POINT ( 'NONE',  ( -82.62287095715005592, -29.50248528299804818, 1.056150453629038477 ) ) ;
#68703=B_SPLINE_CURVE_WITH_KNOTS ( 'NONE', 3,
 ( #24092, #1771, #94611, #39822, #77372, #31206 ),
 .UNSPECIFIED., .F., .F.,
 ( 4, 2, 4 ),
 ( 1.570887131794638196E-05, 0.001396322306279762591, 0.002776935741241578874 ),
 .UNSPECIFIED. ) ;
#68704=CARTESIAN_POINT ( 'NONE',  ( -81.42380231474228935, -29.50249428492551829, 5.197779886230994073 ) ) ;
#68705=CARTESIAN_POINT ( 'NONE',  ( -9.862393454161701101, 16.67994275214481092, -1.500000000000002220 ) ) ;
#68706=CARTESIAN_POINT ( 'NONE',  ( -39.02475006312682382, -25.32724636324322987, 4.398074533285874388 ) ) ;
#68707=VERTEX_POINT ( 'NONE', #28694 ) ;
#68708=CARTESIAN_POINT ( 'NONE',  ( -13.34961138979462270, 14.11212085816309880, 11.49999999999999645 ) ) ;
#68713=CARTESIAN_POINT ( 'NONE',  ( -64.62287095715005592, -29.50247984919015209, -1.443849546365056913 ) ) ;
#68716=CARTESIAN_POINT ( 'NONE',  ( -2.340448316220725467, 19.49152957720520618, 11.49999999999998934 ) ) ;
#68717=AXIS2_PLACEMENT_3D ( 'NONE', #7735, #90481, #99075 ) ;
#68718=CARTESIAN_POINT ( 'NONE',  ( -41.39099037118809576, -25.31583651791034129, 4.532732261260102646 ) ) ;
#68719=ORIENTED_EDGE ( 'NONE', *, *, #47826, .F. ) ;
#68720=CARTESIAN_POINT ( 'NONE',  ( -10.34410514300256523, -18.92461576200269491, 11.49999999999998934 ) ) ;
#68721=CARTESIAN_POINT ( 'NONE',  ( -33.48322934098876402, -24.51419770103157347, 9.386484678747185839 ) ) ;
#68722=CARTESIAN_POINT ( 'NONE',  ( -79.62287095715007013, -24.66019654487199375, 8.947790411086128159 ) ) ;
#68723=CARTESIAN_POINT ( 'NONE',  ( -99.52924129105133488, -25.18439473889998581, 3.929520434774139037 ) ) ;
#68724=CARTESIAN_POINT ( 'NONE',  ( 1.912052097559287844, -22.98750448113701239, -1.500000000000002220 ) ) ;
#68727=CARTESIAN_POINT ( 'NONE',  ( -51.30672089287874371, -25.29249258120279009, 4.255736650380444352 ) ) ;
#68728=CARTESIAN_POINT ( 'NONE',  ( -12.53166870608491479, 15.75175023352509385, 11.49999999999999645 ) ) ;
#68730=CARTESIAN_POINT ( 'NONE',  ( -32.52200297606397328, -23.48786465467240347, 11.44779295918255535 ) ) ;
#68731=CARTESIAN_POINT ( 'NONE',  ( -109.3600771921758223, -25.27538837853246179, 4.143864369237199696 ) ) ;
#68732=DIRECTION ( 'NONE',  ( 0.000000000000000000, 2.173523156925980399E-06, -0.9999999999976378895 ) ) ;
#68733=CARTESIAN_POINT ( 'NONE',  ( -30.93930316463115915, -23.47596703998600276, 11.44779298504227683 ) ) ;
#68735=CARTESIAN_POINT ( 'NONE',  ( 17.36586316225375981, 9.700842922841564686, 11.49999999999998934 ) ) ;
#68736=CARTESIAN_POINT ( 'NONE',  ( -118.5895376238167245, -23.48786465467241769, 11.44779295918253759 ) ) ;
#68737=CARTESIAN_POINT ( 'NONE',  ( 7.891737972721761807, -18.10977644326358771, -1.500000000000002220 ) ) ;
#68738=CARTESIAN_POINT ( 'NONE',  ( -56.59304687066833139, -24.15543982623907127, -0.2315651400026670359 ) ) ;
#68740=CARTESIAN_POINT ( 'NONE',  ( -40.43756433397305727, -25.29116518533085056, 2.832404424262111586 ) ) ;
#68742=CARTESIAN_POINT ( 'NONE',  ( -10.67548511050313209, -17.69376651829569269, 11.49999999999999645 ) ) ;
#68743=CARTESIAN_POINT ( 'NONE',  ( -39.56136241089613037, -25.27985553519108564, 5.536731371927209544 ) ) ;
#68746=CARTESIAN_POINT ( 'NONE',  ( 13.97002500213282516, -17.90638934399130733, 11.49999999999999645 ) ) ;
#68747=EDGE_CURVE ( 'NONE', #29553, #77786, #44765, .T. ) ;
#68750=CARTESIAN_POINT ( 'NONE',  ( -69.74137862423624767, -25.15171692517981583, 6.930849537325211251 ) ) ;
#68751=CARTESIAN_POINT ( 'NONE',  ( -12.46103870137906711, 15.87156016069071462, -1.500000000000002220 ) ) ;
#68752=CARTESIAN_POINT ( 'NONE',  ( -63.54362810327751276, -24.34968618360933235, 0.1864209137778804204 ) ) ;
#68753=CARTESIAN_POINT ( 'NONE',  ( -84.62287095715005592, -29.50248528299804818, 1.056150453629038477 ) ) ;
#68754=ORIENTED_EDGE ( 'NONE', *, *, #48087, .T. ) ;
#68757=CARTESIAN_POINT ( 'NONE',  ( 21.13568926591755925, -8.834425160694816981, -1.500000000000002220 ) ) ;
#68758=CARTESIAN_POINT ( 'NONE',  ( -50.83488094104556154, -25.18439667156625816, 3.373740327774851000 ) ) ;
#68759=CARTESIAN_POINT ( 'NONE',  ( 4.348677445931066643, 21.19853102677161871, -1.500000000000002220 ) ) ;
#68762=CARTESIAN_POINT ( 'NONE',  ( -20.37482282770194075, 4.769447832466558346, 11.49999999999999645 ) ) ;
#68764=CARTESIAN_POINT ( 'NONE',  ( -114.9228709571500673, -23.47596703998600276, 11.44779298504227860 ) ) ;
#68765=CARTESIAN_POINT ( 'NONE',  ( -18.24146354680218707, 12.35505607031776165, -1.500000000000002220 ) ) ;
#68767=EDGE_CURVE ( 'NONE', #34072, #96024, #22058, .T. ) ;
#68768=EDGE_CURVE ( 'NONE', #31190, #98513, #53039, .T. ) ;
#68769=CARTESIAN_POINT ( 'NONE',  ( -105.5507813405130264, -24.52399227489126687, 9.353111116836517525 ) ) ;
#68770=CARTESIAN_POINT ( 'NONE',  ( -28.81656857143860861, -25.21724860399139700, 6.988806608617056604 ) ) ;
#68771=ORIENTED_EDGE ( 'NONE', *, *, #19324, .F. ) ;
#68772=CARTESIAN_POINT ( 'NONE',  ( -73.52287095715007581, -23.47593901973090169, -1.443836447538996870 ) ) ;
#68774=ORIENTED_EDGE ( 'NONE', *, *, #11411, .F. ) ;
#68775=FACE_OUTER_BOUND ( 'NONE', #6375, .T. ) ;
#68776=ORIENTED_EDGE ( 'NONE', *, *, #48369, .T. ) ;
#68777=EDGE_LOOP ( 'NONE', ( #72826, #73762, #27728, #73421 ) ) ;
#68778=CARTESIAN_POINT ( 'NONE',  ( -71.58790182756980869, -24.35071581493543391, 9.817618358456021710 ) ) ;
#68779=FACE_OUTER_BOUND ( 'NONE', #31422, .T. ) ;
#68780=CARTESIAN_POINT ( 'NONE',  ( -57.63796154297044438, -24.15543982623907127, -0.2315651400026663420 ) ) ;
#68781=CARTESIAN_POINT ( 'NONE',  ( 14.46511082492616573, -14.46070965572739730, -1.500000000000002220 ) ) ;
#68782=VECTOR ( 'NONE', #95740, 1000.000000000000114 ) ;
#68785=ADVANCED_FACE ( 'NONE', ( #60160 ), #6845, .T. ) ;
#68786=CARTESIAN_POINT ( 'NONE',  ( -30.63208233338743725, -23.87624887660336981, 11.01174216661999772 ) ) ;
#68788=CARTESIAN_POINT ( 'NONE',  ( -2.790049085472659396, -22.09070898310802633, -1.500000000000002220 ) ) ;
#68789=ADVANCED_FACE ( 'NONE', ( #5851 ), #37801, .T. ) ;
#68791=PLANE ( 'NONE',  #12407 ) ;
#68794=CARTESIAN_POINT ( 'NONE',  ( -28.54076794517382965, -25.26248034578510371, 8.057460879817709198 ) ) ;
#68795=CARTESIAN_POINT ( 'NONE',  ( 20.70993026999094511, 1.908435391604796028, 11.49999999999998934 ) ) ;
#68798=ORIENTED_EDGE ( 'NONE', *, *, #24101, .T. ) ;
#68799=CARTESIAN_POINT ( 'NONE',  ( -119.2228709571500787, -23.47596703998600276, 11.44779298504227683 ) ) ;
#68803=CARTESIAN_POINT ( 'NONE',  ( -50.55649023882089921, -25.10935758318566968, 2.837765538655498077 ) ) ;
#68804=CARTESIAN_POINT ( 'NONE',  ( -77.62287095715005592, -29.50250243563736774, 8.947779886222141599 ) ) ;
#68806=CARTESIAN_POINT ( 'NONE',  ( -92.50938377975539595, -24.35071581493542681, 9.817618358456023486 ) ) ;
#68808=ADVANCED_FACE ( 'NONE', ( #7842 ), #76344, .F. ) ;
#68809=CARTESIAN_POINT ( 'NONE',  ( 2.574831182292884435, -22.01391258260016315, 11.49999999999999645 ) ) ;
#68812=CARTESIAN_POINT ( 'NONE',  ( 5.572475817582897228, 21.94689365879375131, -1.500000000000002220 ) ) ;
#68813=CARTESIAN_POINT ( 'NONE',  ( -124.6228709571500559, -23.47593901973091235, -1.443836447538997536 ) ) ;
#68814=ORIENTED_EDGE ( 'NONE', *, *, #65153, .T. ) ;
#68816=AXIS2_PLACEMENT_3D ( 'NONE', #56769, #94802, #41032 ) ;
#68817=CARTESIAN_POINT ( 'NONE',  ( -112.9228709571500673, -23.47596703998600631, 11.44779298504227860 ) ) ;
#68819=CARTESIAN_POINT ( 'NONE',  ( -8.609638109768802394, 18.19638482192696216, 11.49999999999998934 ) ) ;
#68820=EDGE_CURVE ( 'NONE', #62489, #45200, #77450, .T. ) ;
#68821=B_SPLINE_SURFACE_WITH_KNOTS ( 'NONE', 3, 3, ( 
 ( #65767, #98172, #58143, #42914 ),
 ( #59635, #21047, #52016, #52515 ),
 ( #89080, #4840, #5334, #73853 ),
 ( #82945, #97683, #83446, #91065 ),
 ( #97188, #19556, #20060, #50515 ),
 ( #81473, #35793, #44909, #11947 ),
 ( #59137, #35302, #27683, #51521 ) ),
 .UNSPECIFIED., .F., .F., .F.,
 ( 4, 3, 4 ),
 ( 4, 4 ),
 ( 0.0004766839783825173532, 0.1029713700210899696, 0.2054660560637974198 ),
 ( 0.1695371245961057594, 0.1706280732699167746 ),
 .UNSPECIFIED. ) ;
#68824=CARTESIAN_POINT ( 'NONE',  ( -126.5228709571500616, -24.65952944569305316, 1.056160979905707675 ) ) ;
#68825=CARTESIAN_POINT ( 'NONE',  ( 21.86734719908870872, 4.625976558377421277, -1.500000000000002220 ) ) ;
#68826=EDGE_CURVE ( 'NONE', #20337, #10587, #90768, .T. ) ;
#68828=ORIENTED_EDGE ( 'NONE', *, *, #68134, .T. ) ;
#68830=PLANE ( 'NONE',  #62096 ) ;
#68831=CARTESIAN_POINT ( 'NONE',  ( -60.52287095715006160, -29.50248528299804818, 1.056150453629034924 ) ) ;
#68832=CARTESIAN_POINT ( 'NONE',  ( -119.6228709571500559, -23.47593901973091235, -1.443836447538997536 ) ) ;
#68834=CARTESIAN_POINT ( 'NONE',  ( -73.52287095715007581, -24.64965694238407323, 8.947790433994200043 ) ) ;
#68835=CARTESIAN_POINT ( 'NONE',  ( 19.50827032651345405, -1.201405007418623994, -1.500000000000002220 ) ) ;
#68837=CARTESIAN_POINT ( 'NONE',  ( 5.910897418159350103, -20.63055655796343757, -1.500000000000002220 ) ) ;
#68838=CARTESIAN_POINT ( 'NONE',  ( -25.60037597819128763, -24.57999985355001016, 3.875573678034330616 ) ) ;
#68839=CARTESIAN_POINT ( 'NONE',  ( -120.5228709571500332, -23.85196035786901803, -0.8779234886475113520 ) ) ;
#68841=CARTESIAN_POINT ( 'NONE',  ( -6.237877366497927234, -22.00199818733190327, -1.500000000000002220 ) ) ;
#68844=CARTESIAN_POINT ( 'NONE',  ( -101.9507253916653440, -25.25287247409162816, 6.236250661346385726 ) ) ;
#68846=CARTESIAN_POINT ( 'NONE',  ( -4.560224734120114753, 19.45435480350565882, 11.49999999999999645 ) ) ;
#68848=CARTESIAN_POINT ( 'NONE',  ( -74.54564100032425245, -24.35071581493544102, 9.817618358456019934 ) ) ;
#68850=ORIENTED_EDGE ( 'NONE', *, *, #39792, .F. ) ;
#68851=FACE_OUTER_BOUND ( 'NONE', #7694, .T. ) ;
#68853=CARTESIAN_POINT ( 'NONE',  ( 20.36105213711617878, 7.643125777291208678, 11.49999999999998934 ) ) ;
#68854=CARTESIAN_POINT ( 'NONE',  ( -65.92287095715006728, -23.47596703998600631, 11.44779298504227860 ) ) ;
#68855=CARTESIAN_POINT ( 'NONE',  ( -16.94305004876727239, 9.801747318927828800, -1.500000000000002220 ) ) ;
#68856=PLANE ( 'NONE',  #52308 ) ;
#68857=EDGE_CURVE ( 'NONE', #7606, #22830, #72631, .T. ) ;
#68859=CARTESIAN_POINT ( 'NONE',  ( -30.65075040189094580, -23.47621662958674804, 11.44779298504227683 ) ) ;
#68861=CARTESIAN_POINT ( 'NONE',  ( 17.35315496411208613, -10.91789592880838811, 11.49999999999999645 ) ) ;
#68862=CARTESIAN_POINT ( 'NONE',  ( -94.52287095715006160, -24.64898659630367916, 1.056161002820827921 ) ) ;
#68864=VERTEX_POINT ( 'NONE', #7335 ) ;
#68866=CARTESIAN_POINT ( 'NONE',  ( -40.25588136632453740, -25.28892425241502551, 3.308431897907366359 ) ) ;
#68867=CARTESIAN_POINT ( 'NONE',  ( -125.5209391444894749, -24.15602025860897584, 10.28564288303534013 ) ) ;
#68869=DIRECTION ( 'NONE',  ( 0.000000000000000000, 0.9999999999976377785, 2.173523156925979128E-06 ) ) ;
#68871=CARTESIAN_POINT ( 'NONE',  ( 14.65057173600216345, 17.85730367728733725, 11.49999999999999645 ) ) ;
#68872=CARTESIAN_POINT ( 'NONE',  ( -10.93939140624874007, -20.02795264745160608, -1.500000000000002220 ) ) ;
#68875=CARTESIAN_POINT ( 'NONE',  ( -123.5228709571500616, -24.65952944569304961, 1.056160979905705899 ) ) ;
#68876=VECTOR ( 'NONE', #43287, 1000.000000000000114 ) ;
#68877=CARTESIAN_POINT ( 'NONE',  ( -109.5948960647422723, -25.15277794460069671, 6.986250878905949868 ) ) ;
#68879=CARTESIAN_POINT ( 'NONE',  ( 21.74639208212181529, -2.611101805624240768, -1.500000000000002220 ) ) ;
#68881=EDGE_CURVE ( 'NONE', #6691, #11783, #22548, .T. ) ;
#68882=CARTESIAN_POINT ( 'NONE',  ( -50.62287095715007723, -24.15431212366392444, -0.2830839119429141570 ) ) ;
#68883=CARTESIAN_POINT ( 'NONE',  ( -41.02757408530191441, -25.31561146209963198, 4.926386051049478354 ) ) ;
#68887=CARTESIAN_POINT ( 'NONE',  ( 16.50020720150075348, -12.08490501797973238, -1.500000000000002220 ) ) ;
#68891=ORIENTED_EDGE ( 'NONE', *, *, #31509, .F. ) ;
#68892=CARTESIAN_POINT ( 'NONE',  ( -22.22199965279648737, -6.226755796435518242, 11.49999999999998934 ) ) ;
#68893=CARTESIAN_POINT ( 'NONE',  ( -40.80038310650994759, -25.18341647909762671, 3.283321612209681550 ) ) ;
#68894=CARTESIAN_POINT ( 'NONE',  ( 20.05691770114479766, 3.104179615465487707, -1.500000000000002220 ) ) ;
#68895=ORIENTED_EDGE ( 'NONE', *, *, #22674, .T. ) ;
#68896=EDGE_CURVE ( 'NONE', #48223, #47437, #61662, .T. ) ;
#68897=CARTESIAN_POINT ( 'NONE',  ( -26.08159193753483507, -24.86405713208039359, 6.759032221908315208 ) ) ;
#68899=CARTESIAN_POINT ( 'NONE',  ( -87.62287095715008434, -24.51387760970723306, 9.387446482453421837 ) ) ;
#68901=B_SPLINE_CURVE_WITH_KNOTS ( 'NONE', 3,
 ( #34541, #80209, #88326, #26925, #58878, #10702, #26430, #12685, #43648, #73108, #57894, #3597, #74586, #50767, #66514, #5076 ),
 .UNSPECIFIED., .F., .F.,
 ( 4, 2, 2, 2, 2, 2, 2, 4 ),
 ( 0.000000000000000000, 0.0002571301802276845013, 0.0005142603604553690026, 0.001028520720910736704, 0.001285650901138406677, 0.001542781081366076217, 0.001799911261593746190, 0.002057041441821416163 ),
 .UNSPECIFIED. ) ;
#68902=LINE ( 'NONE', #68408, #85305 ) ;
#68903=CARTESIAN_POINT ( 'NONE',  ( -70.59774629277985980, -24.15503026093916006, -0.2815557561904372674 ) ) ;
#68904=CARTESIAN_POINT ( 'NONE',  ( -17.32345979880200204, -12.59856583755568415, 11.49999999999999645 ) ) ;
#68905=ORIENTED_EDGE ( 'NONE', *, *, #42097, .F. ) ;
#68906=CARTESIAN_POINT ( 'NONE',  ( -100.5562042904834072, -23.47593901973091235, -1.443836447539001089 ) ) ;
#68908=EDGE_CURVE ( 'NONE', #12709, #90732, #24061, .T. ) ;
#68909=ORIENTED_EDGE ( 'NONE', *, *, #3220, .T. ) ;
#68910=CARTESIAN_POINT ( 'NONE',  ( 11.71144010791963730, -17.07555522294065753, -1.500000000000002220 ) ) ;
#68911=AXIS2_PLACEMENT_3D ( 'NONE', #82113, #90226, #5484 ) ;
#68912=EDGE_LOOP ( 'NONE', ( #7986, #39608, #1292, #59081 ) ) ;
#68914=ORIENTED_EDGE ( 'NONE', *, *, #47264, .T. ) ;
#68915=CARTESIAN_POINT ( 'NONE',  ( -28.59443407473934329, -23.99887327325441788, -0.2315644524145782090 ) ) ;
#68918=CARTESIAN_POINT ( 'NONE',  ( -65.48792298204898543, -24.83618233451449697, 1.606449574219540155 ) ) ;
#68919=EDGE_CURVE ( 'NONE', #53307, #40253, #31455, .T. ) ;
#68920=CARTESIAN_POINT ( 'NONE',  ( -21.79611004543898289, 2.820803583321412678, 11.49999999999999645 ) ) ;
#68923=CARTESIAN_POINT ( 'NONE',  ( 4.940617368476682536, -22.01678987175928981, -1.500000000000002220 ) ) ;
#68924=AXIS2_PLACEMENT_3D ( 'NONE', #48575, #86612, #17098 ) ;
#68925=CARTESIAN_POINT ( 'NONE',  ( -3.838044578953509145, 20.63102806057878880, -1.500000000000002220 ) ) ;
#68926=DIRECTION ( 'NONE',  ( -3.773278334453079030E-23, 0.9999999999976377785, 2.173523156925979128E-06 ) ) ;
#68930=ORIENTED_EDGE ( 'NONE', *, *, #99782, .T. ) ;
#68932=CARTESIAN_POINT ( 'NONE',  ( -88.52287095715006160, -24.33927499327854349, 9.819080762295801179 ) ) ;
#68934=CARTESIAN_POINT ( 'NONE',  ( 11.68953838083566588, 18.09531432177502808, -1.500000000000002220 ) ) ;
#68935=B_SPLINE_CURVE_WITH_KNOTS ( 'NONE', 3,
 ( #32782, #63762, #58627, #13931, #83947, #12438 ),
 .UNSPECIFIED., .F., .F.,
 ( 4, 2, 4 ),
 ( 6.384118678607784034E-06, 0.001386860460828371082, 0.002767336802978134086 ),
 .UNSPECIFIED. ) ;
#68936=CARTESIAN_POINT ( 'NONE',  ( -105.5228709571500616, -24.51254535375846189, 9.355368624242128561 ) ) ;
#68938=CARTESIAN_POINT ( 'NONE',  ( -18.40674794014382698, -10.35651468716735657, -1.500000000000002220 ) ) ;
#68939=FACE_OUTER_BOUND ( 'NONE', #8066, .T. ) ;
#68940=CARTESIAN_POINT ( 'NONE',  ( -64.64729366872971639, -23.73766607897670156, -1.055555164236459564 ) ) ;
#68944=CARTESIAN_POINT ( 'NONE',  ( 12.10043277420606778, 18.60588626676543100, -1.500000000000002220 ) ) ;
#68945=CARTESIAN_POINT ( 'NONE',  ( -40.52287095715006870, -23.47593901973090169, -1.443836447538997092 ) ) ;
#68946=EDGE_CURVE ( 'NONE', #95392, #76295, #85969, .T. ) ;
#68947=ORIENTED_EDGE ( 'NONE', *, *, #36647, .F. ) ;
#68948=CARTESIAN_POINT ( 'NONE',  ( -51.81420417462592809, -25.31633237273065618, 5.643201719655072779 ) ) ;
#68949=CARTESIAN_POINT ( 'NONE',  ( -67.62287095715005592, -24.64898659630367916, 1.056161002820824368 ) ) ;
#68951=EDGE_CURVE ( 'NONE', #46913, #62281, #3616, .T. ) ;
#68953=CARTESIAN_POINT ( 'NONE',  ( 1.255614643274026276, -19.41590359075080841, -1.500000000000002220 ) ) ;
#68954=VECTOR ( 'NONE', #48164, 1000.000000000000114 ) ;
#68955=CARTESIAN_POINT ( 'NONE',  ( -21.18999663186871274, 2.814949255606389311, -1.500000000000002220 ) ) ;
#68957=CARTESIAN_POINT ( 'NONE',  ( -90.70915032798693289, -25.26877915520014639, 5.947789088310639904 ) ) ;
#68960=CARTESIAN_POINT ( 'NONE',  ( -9.076218414377828836, -20.82814578352222767, -1.500000000000002220 ) ) ;
#68961=ORIENTED_EDGE ( 'NONE', *, *, #74513, .T. ) ;
#68962=FACE_OUTER_BOUND ( 'NONE', #22461, .T. ) ;
#68963=CARTESIAN_POINT ( 'NONE',  ( -62.62287095715004881, -23.73934037231756733, 11.05740245334329153 ) ) ;
#68964=CARTESIAN_POINT ( 'NONE',  ( -17.91562471463183570, -8.470225615102204841, 11.49999999999999645 ) ) ;
#68968=CARTESIAN_POINT ( 'NONE',  ( -75.52287095715009002, -24.83620972994592435, 8.398175272781367440 ) ) ;
#68969=CARTESIAN_POINT ( 'NONE',  ( 18.46943957830784555, -11.30625484363265265, 11.49999999999998934 ) ) ;
#68971=CARTESIAN_POINT ( 'NONE',  ( -7.106217341473486826, 18.08270997100935418, -1.500000000000002220 ) ) ;
#68972=DIRECTION ( 'NONE',  ( 0.000000000000000000, -0.9999999999976377785, -2.173523156925979975E-06 ) ) ;
#68973=CARTESIAN_POINT ( 'NONE',  ( -82.62287095715005592, -23.48786465467241413, 11.44779295918254647 ) ) ;
#68974=CARTESIAN_POINT ( 'NONE',  ( 6.388261542594571019, -18.74682169789839392, 11.49999999999998934 ) ) ;
#68975=B_SPLINE_CURVE_WITH_KNOTS ( 'NONE', 3,
 ( #100196, #92111, #93104, #22579 ),
 .UNSPECIFIED., .F., .F.,
 ( 4, 4 ),
 ( 0.000000000000000000, 0.0001000000000000028644 ),
 .UNSPECIFIED. ) ;
#68977=CARTESIAN_POINT ( 'NONE',  ( -12.35269427871797987, -16.12754648828645543, 11.49999999999999645 ) ) ;
#68978=DIRECTION ( 'NONE',  ( -1.000000000000000000, -3.773278334444166432E-23, -8.201307841325785021E-29 ) ) ;
#68981=FACE_OUTER_BOUND ( 'NONE', #60921, .T. ) ;
#68982=VERTEX_POINT ( 'NONE', #71252 ) ;
#68983=CARTESIAN_POINT ( 'NONE',  ( -30.59128290392954597, -24.93418366566757882, 8.369064737642425200 ) ) ;
#68984=FACE_OUTER_BOUND ( 'NONE', #47859, .T. ) ;
#68985=CARTESIAN_POINT ( 'NONE',  ( -49.63502199369077772, -25.25214439884339157, 4.997542013878374156 ) ) ;
#68987=CARTESIAN_POINT ( 'NONE',  ( -40.64475957891966118, -24.40133493613049609, 9.663955038902802386 ) ) ;
#68989=CARTESIAN_POINT ( 'NONE',  ( -127.6228709571500559, -24.64965695001469115, 8.947790433994173398 ) ) ;
#68990=CARTESIAN_POINT ( 'NONE',  ( -19.29710791919172053, 5.528754708966634901, 11.49999999999998934 ) ) ;
#68992=CARTESIAN_POINT ( 'NONE',  ( -74.62287095715005592, -23.47593901973091235, -1.443836447539006196 ) ) ;
#68996=CARTESIAN_POINT ( 'NONE',  ( -22.23020047961643186, 5.420056861400933457, 11.49999999999999645 ) ) ;
#68997=CARTESIAN_POINT ( 'NONE',  ( -20.99730734726578874, -8.693733401623333634, -1.500000000000002220 ) ) ;
#68998=CARTESIAN_POINT ( 'NONE',  ( -30.47287095715008576, -23.78427885734157954, -0.9431990486725588818 ) ) ;
#68999=CARTESIAN_POINT ( 'NONE',  ( -97.55620429048340725, -23.47593901973091235, -1.443836447539001089 ) ) ;
#69000=CARTESIAN_POINT ( 'NONE',  ( -38.52201939144443799, -23.48786465467240347, 11.44779295918255002 ) ) ;
#69001=CARTESIAN_POINT ( 'NONE',  ( -108.5228709571500758, -23.47593901973090524, -1.443836447538996204 ) ) ;
#69003=LINE ( 'NONE', #46173, #59858 ) ;
#69004=ORIENTED_EDGE ( 'NONE', *, *, #28822, .F. ) ;
#69005=EDGE_CURVE ( 'NONE', #65202, #84765, #54466, .T. ) ;
#69006=CARTESIAN_POINT ( 'NONE',  ( 20.27773211485958527, -1.686570798567030183, -1.500000000000002220 ) ) ;
#69007=ORIENTED_EDGE ( 'NONE', *, *, #38598, .T. ) ;
#69008=EDGE_CURVE ( 'NONE', #65701, #6520, #88255, .T. ) ;
#69009=CARTESIAN_POINT ( 'NONE',  ( -10.52143791818333085, 20.43947972196396989, -1.500000000000002220 ) ) ;
#69010=DIRECTION ( 'NONE',  ( 0.000000000000000000, -2.173523156925979552E-06, 0.9999999999976378895 ) ) ;
#69012=ORIENTED_EDGE ( 'NONE', *, *, #92299, .F. ) ;
#69014=EDGE_CURVE ( 'NONE', #87739, #62329, #83378, .T. ) ;
#69017=CARTESIAN_POINT ( 'NONE',  ( -51.55335675300738529, -23.96169478059712787, 10.65365249895718236 ) ) ;
#69018=CARTESIAN_POINT ( 'NONE',  ( 17.84191302092929021, 11.53353326677314961, 11.49999999999999645 ) ) ;
#69019=ORIENTED_EDGE ( 'NONE', *, *, #87170, .F. ) ;
#69020=B_SPLINE_CURVE_WITH_KNOTS ( 'NONE', 3,
 ( #4090, #88831, #19299, #20286 ),
 .UNSPECIFIED., .F., .F.,
 ( 4, 4 ),
 ( 0.000000000000000000, 0.0001000000000000167422 ),
 .UNSPECIFIED. ) ;
#69022=CARTESIAN_POINT ( 'NONE',  ( 4.129723114849880083, -21.82631191821171512, 11.49999999999998934 ) ) ;
#69023=CARTESIAN_POINT ( 'NONE',  ( -15.36756058500021282, 13.76162614515376426, 11.49999999999998934 ) ) ;
#69024=VERTEX_POINT ( 'NONE', #73744 ) ;
#69026=CARTESIAN_POINT ( 'NONE',  ( -109.8219511710470897, -25.31627459236276323, 5.738454807850723149 ) ) ;
#69027=CARTESIAN_POINT ( 'NONE',  ( -40.34542624296162927, -25.12112790398598605, 2.835882484633130307 ) ) ;
#69031=CARTESIAN_POINT ( 'NONE',  ( -89.40841769935767047, -25.22391154813773895, 6.409327647370974823 ) ) ;
#69032=CARTESIAN_POINT ( 'NONE',  ( -35.55620429048339304, -23.48786465467240347, 11.44779295918255180 ) ) ;
#69033=CARTESIAN_POINT ( 'NONE',  ( 14.06386034339543478, -15.33156129944631729, -1.500000000000002220 ) ) ;
#69034=CARTESIAN_POINT ( 'NONE',  ( 10.97640485992876691, 18.82695874702771377, 11.49999999999999645 ) ) ;
#69035=CARTESIAN_POINT ( 'NONE',  ( -40.81961785418572930, -25.31583757272871082, 5.018035748688583375 ) ) ;
#69037=CARTESIAN_POINT ( 'NONE',  ( -8.346146134265904237, -20.86121191590761015, -1.500000000000002220 ) ) ;
#69039=CARTESIAN_POINT ( 'NONE',  ( -38.52287095715006870, -23.47593901973090169, -1.443836447538997092 ) ) ;
#69040=VERTEX_POINT ( 'NONE', #18954 ) ;
#69042=CARTESIAN_POINT ( 'NONE',  ( -101.5468792378191978, -25.24282061761980955, 6.236250683194342059 ) ) ;
#69043=EDGE_CURVE ( 'NONE', #70639, #35626, #47106, .T. ) ;
#69045=ORIENTED_EDGE ( 'NONE', *, *, #39711, .T. ) ;
#69046=ORIENTED_EDGE ( 'NONE', *, *, #8362, .F. ) ;
#69048=CARTESIAN_POINT ( 'NONE',  ( -15.71168838272081558, 14.50144224353281786, -1.500000000000002220 ) ) ;
#69051=CARTESIAN_POINT ( 'NONE',  ( -14.96386864383857329, 14.77685607883014640, -1.500000000000002220 ) ) ;
#69052=CARTESIAN_POINT ( 'NONE',  ( -30.46621203179166670, -25.14181536550043461, 2.712646531854225440 ) ) ;
#69053=CARTESIAN_POINT ( 'NONE',  ( -110.4037686302767867, -25.19528510359861073, 3.295747964419194709 ) ) ;
#69056=CARTESIAN_POINT ( 'NONE',  ( 20.22059317821533853, 8.664326447042464352, -1.500000000000002220 ) ) ;
#69059=CARTESIAN_POINT ( 'NONE',  ( -30.64427850938831099, -23.56000036390796382, 11.50200000000000067 ) ) ;
#69062=EDGE_CURVE ( 'NONE', #42104, #8769, #81859, .T. ) ;
#69063=CARTESIAN_POINT ( 'NONE',  ( -84.63607584393763261, -23.96169478059713498, 10.65365249895717881 ) ) ;
#69064=CARTESIAN_POINT ( 'NONE',  ( -127.5228709571500616, -23.47596703998600631, 11.44779298504227683 ) ) ;
#69065=CARTESIAN_POINT ( 'NONE',  ( -0.05081623857416547180, -22.39214385819346376, 8.640809912072077381 ) ) ;
#69066=CARTESIAN_POINT ( 'NONE',  ( 20.09692647535021948, 7.048664716645152595, 11.49999999999998934 ) ) ;
#69067=CARTESIAN_POINT ( 'NONE',  ( -29.62287095715004881, -24.57400415421967566, 8.947790463233827651 ) ) ;
#69068=CARTESIAN_POINT ( 'NONE',  ( -27.61766922344000363, -24.97064402808534567, 2.278554500308590303 ) ) ;
#69070=CARTESIAN_POINT ( 'NONE',  ( -122.5562042904834072, -24.65952944569305316, 1.056160979905704789 ) ) ;
#69071=CARTESIAN_POINT ( 'NONE',  ( -85.62287095715005592, -23.47596703998600631, 11.44779298504227860 ) ) ;
#69072=CARTESIAN_POINT ( 'NONE',  ( -16.74547196562220464, 15.07928529822544661, -1.500000000000002220 ) ) ;
#69073=CARTESIAN_POINT ( 'NONE',  ( -109.9079352936591931, -25.32390614315827193, 4.358500768180118889 ) ) ;
#69076=CARTESIAN_POINT ( 'NONE',  ( 6.560884470684795744, 18.50665934316380756, 11.49999999999999645 ) ) ;
#69077=CARTESIAN_POINT ( 'NONE',  ( -81.62287095715005592, -29.50247984919015209, -1.443849546365053582 ) ) ;
#69078=CARTESIAN_POINT ( 'NONE',  ( -100.6228709571500701, -24.91570333823099759, 8.075032458375556388 ) ) ;
#69080=CARTESIAN_POINT ( 'NONE',  ( -69.38891176720768783, -25.30450784505188011, 5.175863248522402316 ) ) ;
#69081=CARTESIAN_POINT ( 'NONE',  ( -84.55620429048339304, -23.47593901973091235, -1.443836447539004642 ) ) ;
#69083=CARTESIAN_POINT ( 'NONE',  ( -0.6023826358649750912, 19.72334862104828090, -1.500000000000002220 ) ) ;
#69084=B_SPLINE_CURVE_WITH_KNOTS ( 'NONE', 3,
 ( #68224, #60124, #27668, #43888 ),
 .UNSPECIFIED., .F., .F.,
 ( 4, 4 ),
 ( 0.000000000000000000, 9.999999999998897304E-05 ),
 .UNSPECIFIED. ) ;
#69087=DIRECTION ( 'NONE',  ( 0.000000000000000000, -2.173523156925979552E-06, 0.9999999999976378895 ) ) ;
#69089=EDGE_LOOP ( 'NONE', ( #65703, #55054, #4508, #66581 ) ) ;
#69090=CARTESIAN_POINT ( 'NONE',  ( -124.5228709571500616, -24.50321055353805733, 9.387540953477520489 ) ) ;
#69093=DIRECTION ( 'NONE',  ( -3.773278334453079030E-23, 0.9999999999976377785, 2.173523156925979128E-06 ) ) ;
#69095=CARTESIAN_POINT ( 'NONE',  ( -67.55620429048340725, -24.64965694238574656, 8.947790433994198267 ) ) ;
#69097=CARTESIAN_POINT ( 'NONE',  ( -19.61284664649099696, 3.773188449817356904, 11.49999999999998934 ) ) ;
#69098=CARTESIAN_POINT ( 'NONE',  ( -100.2631815169052203, -25.27532862745151121, 2.837685666037238708 ) ) ;
#69099=CARTESIAN_POINT ( 'NONE',  ( -45.53465330854339044, -24.63419186844611630, 9.035850630976932862 ) ) ;
#69100=ORIENTED_EDGE ( 'NONE', *, *, #93583, .F. ) ;
#69102=B_SPLINE_CURVE_WITH_KNOTS ( 'NONE', 3,
 ( #89307, #26905, #81695, #22138 ),
 .UNSPECIFIED., .F., .F.,
 ( 4, 4 ),
 ( 0.9711935055097813407, 0.9801999367818968745 ),
 .UNSPECIFIED. ) ;
#69104=CARTESIAN_POINT ( 'NONE',  ( -80.54796053850395765, -24.40133493613049964, 9.663955038902802386 ) ) ;
#69105=FACE_OUTER_BOUND ( 'NONE', #1002, .T. ) ;
#69107=CARTESIAN_POINT ( 'NONE',  ( -71.62287095715005592, -24.64898659630528854, 1.056161002820824368 ) ) ;
#69109=CARTESIAN_POINT ( 'NONE',  ( -37.62287095715004170, -23.95044443724991368, 10.65354141964649237 ) ) ;
#69110=DIRECTION ( 'NONE',  ( -3.773278334453079030E-23, 0.9999999999976377785, 2.173523156925979128E-06 ) ) ;
#69111=VECTOR ( 'NONE', #37835, 1000.000000000000114 ) ;
#69112=ORIENTED_EDGE ( 'NONE', *, *, #65627, .T. ) ;
#69113=ADVANCED_FACE ( 'NONE', ( #67153 ), #18458, .F. ) ;
#69115=CARTESIAN_POINT ( 'NONE',  ( 2.300710779914242110, 20.15441874099239783, 11.49999999999998934 ) ) ;
#69117=CARTESIAN_POINT ( 'NONE',  ( -76.62287095715005592, -23.96177878511308990, 10.65340807706330395 ) ) ;
#69119=ADVANCED_FACE ( 'NONE', ( #80864 ), #49934, .T. ) ;
#69120=VECTOR ( 'NONE', #51352, 1000.000000000000114 ) ;
#69121=CARTESIAN_POINT ( 'NONE',  ( -90.52287095715003318, -24.51163499207180507, 0.6490370598555487147 ) ) ;
#69124=FACE_OUTER_BOUND ( 'NONE', #43989, .T. ) ;
#69125=CARTESIAN_POINT ( 'NONE',  ( 14.11618873683251252, 14.29484301466228047, -1.500000000000002220 ) ) ;
#69127=CARTESIAN_POINT ( 'NONE',  ( 9.758084087097168791, -18.66043984184860349, 11.49999999999999645 ) ) ;
#69128=CARTESIAN_POINT ( 'NONE',  ( -64.52287095715010423, -24.66019654487200441, 8.947790411086119278 ) ) ;
#69129=CARTESIAN_POINT ( 'NONE',  ( 6.025212951983072607, -21.27585971943098642, 11.49999999999998934 ) ) ;
#69131=CARTESIAN_POINT ( 'NONE',  ( 15.21836549854886123, 13.79734045396011943, 11.49999999999998934 ) ) ;
#69132=FACE_OUTER_BOUND ( 'NONE', #32674, .T. ) ;
#69133=CARTESIAN_POINT ( 'NONE',  ( -126.6228709571500559, -23.72747288104470798, -1.053458166803224794 ) ) ;
#69135=CARTESIAN_POINT ( 'NONE',  ( -87.52287095715006160, -29.50250243563736774, 8.947779886222139822 ) ) ;
#69138=CARTESIAN_POINT ( 'NONE',  ( -64.55620429048337883, -24.64965694238574301, 8.947790433994201820 ) ) ;
#69140=VERTEX_POINT ( 'NONE', #20442 ) ;
#69145=ADVANCED_FACE ( 'NONE', ( #97576 ), #58042, .F. ) ;
#69146=CARTESIAN_POINT ( 'NONE',  ( -13.08992234710881064, 15.94516925376868244, -1.500000000000002220 ) ) ;
#69147=CARTESIAN_POINT ( 'NONE',  ( -16.79864850723062020, -13.61054813162024679, 11.49999999999999645 ) ) ;
#69148=VERTEX_POINT ( 'NONE', #19450 ) ;
#69149=LINE ( 'NONE', #38694, #85554 ) ;
#69152=CARTESIAN_POINT ( 'NONE',  ( -18.60458529277170214, -12.42720982490441095, 11.49999999999998934 ) ) ;
#69153=CARTESIAN_POINT ( 'NONE',  ( -93.52287095715007581, -23.94994826722565762, -0.6494450866342732498 ) ) ;
#69154=CARTESIAN_POINT ( 'NONE',  ( -84.62620519360169169, -24.51314013834316441, 0.6176544820404183955 ) ) ;
#69155=ORIENTED_EDGE ( 'NONE', *, *, #17492, .T. ) ;
#69156=DIRECTION ( 'NONE',  ( 0.000000000000000000, 0.9999999999976377785, 2.173523156925979975E-06 ) ) ;
#69157=CARTESIAN_POINT ( 'NONE',  ( -35.62660692631806114, -24.92592662359561118, 8.075495903017992916 ) ) ;
#69158=CARTESIAN_POINT ( 'NONE',  ( -115.5228709571500616, -24.99132157543084531, 2.256160258750667502 ) ) ;
#69160=CARTESIAN_POINT ( 'NONE',  ( -18.75169668496848985, 9.291489096422434812, 11.49999999999998934 ) ) ;
#69162=B_SPLINE_CURVE_WITH_KNOTS ( 'NONE', 3,
 ( #98142, #50493, #52492, #66239, #81445, #83420 ),
 .UNSPECIFIED., .F., .F.,
 ( 4, 2, 4 ),
 ( 0.000000000000000000, 0.001380764517854766050, 0.002761529035709532100 ),
 .UNSPECIFIED. ) ;
#69163=CARTESIAN_POINT ( 'NONE',  ( -86.62608619482172401, -24.51314013834315375, 0.6176544820404177294 ) ) ;
#69165=ORIENTED_EDGE ( 'NONE', *, *, #49336, .T. ) ;
#69166=CARTESIAN_POINT ( 'NONE',  ( -109.6247146858308952, -24.51419770103157347, 9.386484678747171628 ) ) ;
#69167=CARTESIAN_POINT ( 'NONE',  ( 21.18767802922067034, -0.7184367399587067160, -1.500000000000002220 ) ) ;
#69169=CARTESIAN_POINT ( 'NONE',  ( -118.5228709571500758, -24.65952944569305316, 1.056160979905705899 ) ) ;
#69170=CARTESIAN_POINT ( 'NONE',  ( -99.33919073176147663, -25.26221170829777307, 6.423374375703298611 ) ) ;
#69171=CARTESIAN_POINT ( 'NONE',  ( 20.57308398666954119, -7.222494929537193187, 11.49999999999998934 ) ) ;
#69172=CARTESIAN_POINT ( 'NONE',  ( -89.40841769935767047, -25.22391154813773895, 6.409327647370974823 ) ) ;
#69173=CARTESIAN_POINT ( 'NONE',  ( -55.62287095715005592, -29.50250243563736774, 8.947779886222145151 ) ) ;
#69175=CARTESIAN_POINT ( 'NONE',  ( 8.107222467604051630, 20.28165043084963060, -1.500000000000002220 ) ) ;
#69176=CARTESIAN_POINT ( 'NONE',  ( -71.49027787591442973, -25.31639574635540058, 5.369049132701282367 ) ) ;
#69183=VERTEX_POINT ( 'NONE', #44801 ) ;
#69186=CARTESIAN_POINT ( 'NONE',  ( 9.480266252741309074, -18.97159823121752709, -1.500000000000002220 ) ) ;
#69188=CARTESIAN_POINT ( 'NONE',  ( -130.5728709571500588, -24.13759587396042150, -0.5132947483565719615 ) ) ;
#69192=CARTESIAN_POINT ( 'NONE',  ( -14.46832242630667942, -12.86894606327920876, -1.500000000000002220 ) ) ;
#69194=CARTESIAN_POINT ( 'NONE',  ( -45.67376222244715933, -23.48783264082476663, -1.443836473390103237 ) ) ;
#69195=VERTEX_POINT ( 'NONE', #7719 ) ;
#69196=VECTOR ( 'NONE', #57956, 1000.000000000000114 ) ;
#69197=CARTESIAN_POINT ( 'NONE',  ( -19.16120753946698585, -3.443109951913609024, 11.49999999999999645 ) ) ;
#69198=DIRECTION ( 'NONE',  ( -3.773278334453079618E-23, 0.9999999999976377785, 2.173523156925979975E-06 ) ) ;
#69200=DIRECTION ( 'NONE',  ( 0.8243327689506978473, -1.230443507394594390E-06, 0.5661055431918692316 ) ) ;
#69203=CARTESIAN_POINT ( 'NONE',  ( -78.58953762381672448, -23.47596703998600276, 11.44779298504227683 ) ) ;
#69204=CARTESIAN_POINT ( 'NONE',  ( -59.52287095715006160, -23.48786465467241769, 11.44779295918254824 ) ) ;
#69205=B_SPLINE_CURVE_WITH_KNOTS ( 'NONE', 3,
 ( #89578, #28179, #13936, #66265 ),
 .UNSPECIFIED., .F., .F.,
 ( 4, 4 ),
 ( 0.000000000000000000, 9.999999999998898659E-05 ),
 .UNSPECIFIED. ) ;
#69206=CARTESIAN_POINT ( 'NONE',  ( -61.64687923781919920, -29.50248939449842922, 2.947779886236309377 ) ) ;
#69207=CARTESIAN_POINT ( 'NONE',  ( -93.59418282098891950, -23.96169478059713498, 10.65365249895717170 ) ) ;
#69208=CARTESIAN_POINT ( 'NONE',  ( 19.58216393897113505, 1.562425146961006650, -1.500000000000002220 ) ) ;
#69211=CARTESIAN_POINT ( 'NONE',  ( 2.580163054138214562, 21.43444414123800712, 11.49999999999998934 ) ) ;
#69212=CARTESIAN_POINT ( 'NONE',  ( -95.52287095715007581, -24.63345952396256067, 9.038047939301502964 ) ) ;
#69213=CARTESIAN_POINT ( 'NONE',  ( -40.63310824160917889, -24.73486907724916861, 1.287355809206965240 ) ) ;
#69214=CARTESIAN_POINT ( 'NONE',  ( -90.52287095715003318, -25.00182538069145366, 7.747789668545104647 ) ) ;
#69215=CARTESIAN_POINT ( 'NONE',  ( -6.685540227124203483, -22.02754839873749404, -1.500000000000002220 ) ) ;
#69218=CARTESIAN_POINT ( 'NONE',  ( -93.59740075403963999, -23.73766607897670511, -1.055555164236453791 ) ) ;
#69220=CARTESIAN_POINT ( 'NONE',  ( -2.107266074560359748, -20.09985696230311447, 11.49999999999999645 ) ) ;
#69221=CARTESIAN_POINT ( 'NONE',  ( -33.52287095715006160, -23.48786465467240347, 11.44779295918255357 ) ) ;
#69224=CARTESIAN_POINT ( 'NONE',  ( -110.3641915914744800, -25.10921374192945166, 2.833513679721968881 ) ) ;
#69225=CARTESIAN_POINT ( 'NONE',  ( -126.6228709571500843, -23.47596703998600631, 11.44779298504227860 ) ) ;
#69226=CARTESIAN_POINT ( 'NONE',  ( -111.2332490450528582, -25.29779265843440328, 3.802241964366937399 ) ) ;
#69227=CARTESIAN_POINT ( 'NONE',  ( 4.721227339208565965, -19.33841413273825793, 11.49999999999998934 ) ) ;
#69229=CARTESIAN_POINT ( 'NONE',  ( 18.24360591643979035, -7.691401616277519615, -1.500000000000002220 ) ) ;
#69230=VECTOR ( 'NONE', #61583, 1000.000000000000114 ) ;
#69231=CARTESIAN_POINT ( 'NONE',  ( -56.61227192276419373, -23.48783264082477018, -1.443836473390095909 ) ) ;
#69232=CARTESIAN_POINT ( 'NONE',  ( -40.37522208020789805, -25.10925592908469284, 2.834757886433481033 ) ) ;
#69234=CARTESIAN_POINT ( 'NONE',  ( -19.01758589260300525, -8.224767016273846210, 11.49999999999999645 ) ) ;
#69236=CARTESIAN_POINT ( 'NONE',  ( -115.5228709571500616, -29.50250786944525672, 11.44777988621622811 ) ) ;
#69237=CARTESIAN_POINT ( 'NONE',  ( -49.95596087352405590, -25.31439292586784262, 5.268391321001662853 ) ) ;
#69238=CARTESIAN_POINT ( 'NONE',  ( -12.51292883401962541, 18.98408452820241266, 11.49999999999999645 ) ) ;
#69239=EDGE_LOOP ( 'NONE', ( #69481, #95652, #53926, #61792 ) ) ;
#69240=B_SPLINE_SURFACE_WITH_KNOTS ( 'NONE', 3, 3, ( 
 ( #79027, #41486, #79536, #88661 ),
 ( #40483, #17134, #19130, #32871 ),
 ( #50102, #11520, #34869, #73435 ),
 ( #25247, #3932, #64346, #95762 ),
 ( #2425, #63844, #96762, #40985 ),
 ( #49108, #56220, #33358, #25754 ),
 ( #27261, #86648, #87150, #95264 ) ),
 .UNSPECIFIED., .F., .F., .F.,
 ( 4, 3, 4 ),
 ( 4, 4 ),
 ( 0.0004766839783819443524, 0.1029713700210896227, 0.2054660560637973088 ),
 ( 0.2695625693603935225, 0.2706996695906280781 ),
 .UNSPECIFIED. ) ;
#69241=DIRECTION ( 'NONE',  ( -1.000000000000000000, -3.773278334444167608E-23, -8.201307833595939069E-29 ) ) ;
#69242=DIRECTION ( 'NONE',  ( -3.773278334453079618E-23, 0.9999999999976377785, 2.173523156925978705E-06 ) ) ;
#69243=B_SPLINE_CURVE_WITH_KNOTS ( 'NONE', 3,
 ( #13796, #69090, #53881, #582, #84813, #75695 ),
 .UNSPECIFIED., .F., .F.,
 ( 4, 2, 4 ),
 ( 0.000000000000000000, 0.001380901958385394833, 0.002761803916770789666 ),
 .UNSPECIFIED. ) ;
#69244=CARTESIAN_POINT ( 'NONE',  ( 12.02422309597069017, 16.21794576832014556, -1.500000000000002220 ) ) ;
#69245=CARTESIAN_POINT ( 'NONE',  ( -114.6228709571500559, -29.50247984919015209, -1.443849546365048253 ) ) ;
#69246=DIRECTION ( 'NONE',  ( 3.773278334444166432E-23, -1.000000000000000000, 0.000000000000000000 ) ) ;
#69250=DIRECTION ( 'NONE',  ( -3.773278334444167608E-23, 1.000000000000000000, 0.000000000000000000 ) ) ;
#69251=CARTESIAN_POINT ( 'NONE',  ( 16.30191990219073972, -16.09819076282585826, -1.500000000000002220 ) ) ;
#69252=CARTESIAN_POINT ( 'NONE',  ( -51.10270014058699672, -25.27420619311879335, 3.552653933812367715 ) ) ;
#69253=CARTESIAN_POINT ( 'NONE',  ( -12.93760099376155104, 17.33828479246177423, -1.500000000000002220 ) ) ;
#69254=CARTESIAN_POINT ( 'NONE',  ( -123.6248516269914859, -24.15543982623907482, -0.2315651400026560169 ) ) ;
#69255=CARTESIAN_POINT ( 'NONE',  ( -34.54553770641572896, -24.15543982623907127, -0.2315651400026575435 ) ) ;
#69256=ADVANCED_FACE ( 'NONE', ( #46287 ), #29557, .T. ) ;
#69257=CARTESIAN_POINT ( 'NONE',  ( -20.86263692406621928, 1.606387762444034362, 11.49999999999999645 ) ) ;
#69258=ORIENTED_EDGE ( 'NONE', *, *, #30062, .T. ) ;
#69259=CARTESIAN_POINT ( 'NONE',  ( -115.5228709571500616, -23.47596703998600631, 11.44779298504227860 ) ) ;
#69260=CARTESIAN_POINT ( 'NONE',  ( -0.4018715335629812202, -22.01094342083549193, 11.49999999999998934 ) ) ;
#69262=VECTOR ( 'NONE', #41460, 1000.000000000000114 ) ;
#69264=CARTESIAN_POINT ( 'NONE',  ( -40.43756433397305727, -25.10925768246707435, 2.832404819642281524 ) ) ;
#69265=ORIENTED_EDGE ( 'NONE', *, *, #75310, .T. ) ;
#69268=VERTEX_POINT ( 'NONE', #51915 ) ;
#69269=CARTESIAN_POINT ( 'NONE',  ( -72.62691082383823016, -24.51419770103156281, 9.386484678747185839 ) ) ;
#69272=VERTEX_POINT ( 'NONE', #21929 ) ;
#69273=CARTESIAN_POINT ( 'NONE',  ( -71.51636059175528715, -23.73791477778911840, 11.05961554403170766 ) ) ;
#69275=CARTESIAN_POINT ( 'NONE',  ( -61.62287095715004881, -23.48783264082478439, -1.443836473390069042 ) ) ;
#69276=EDGE_CURVE ( 'NONE', #59593, #81901, #91955, .T. ) ;
#69277=CARTESIAN_POINT ( 'NONE',  ( 5.889875310795558150, 19.62242631308348706, -1.500000000000002220 ) ) ;
#69278=EDGE_LOOP ( 'NONE', ( #43202, #7649, #59198, #60183 ) ) ;
#69280=CARTESIAN_POINT ( 'NONE',  ( -44.48768996415131483, -24.51314013834316086, 0.6176544820404110681 ) ) ;
#69281=CARTESIAN_POINT ( 'NONE',  ( -124.5228709571500616, -29.50250243563736774, 8.947779886222134493 ) ) ;
#69282=CARTESIAN_POINT ( 'NONE',  ( 15.07672925556244969, 16.42598562245719407, -1.500000000000002220 ) ) ;
#69283=DIRECTION ( 'NONE',  ( -3.773278334453079030E-23, 0.9999999999976377785, 2.173523156925979128E-06 ) ) ;
#69284=CARTESIAN_POINT ( 'NONE',  ( -28.55620429048338949, -24.49160925498320296, 8.947790452558288976 ) ) ;
#69287=CARTESIAN_POINT ( 'NONE',  ( -29.26673851950083716, -24.93593727437086471, 2.461460217553469665 ) ) ;
#69288=CARTESIAN_POINT ( 'NONE',  ( -29.66400988275576367, -24.63645681146989119, 6.487136769355695165 ) ) ;
#69289=CARTESIAN_POINT ( 'NONE',  ( -20.61801493038525379, 2.926015819835423581, -1.500000000000002220 ) ) ;
#69290=VERTEX_POINT ( 'NONE', #75233 ) ;
#69292=ORIENTED_EDGE ( 'NONE', *, *, #17447, .F. ) ;
#69293=CARTESIAN_POINT ( 'NONE',  ( -50.56357725185049645, -25.25854568647407206, 7.098062045694851996 ) ) ;
#69294=ORIENTED_EDGE ( 'NONE', *, *, #30413, .F. ) ;
#69297=CARTESIAN_POINT ( 'NONE',  ( -50.38191529551148307, -25.27412227713961457, 2.832404461305267240 ) ) ;
#69298=CARTESIAN_POINT ( 'NONE',  ( -111.3758925029758871, -25.19402559689468646, 6.830252627919830566 ) ) ;
#69300=CARTESIAN_POINT ( 'NONE',  ( -109.7069964148890904, -25.14173549452716472, 2.952782056881928963 ) ) ;
#69302=CARTESIAN_POINT ( 'NONE',  ( -15.83042281971428977, -15.45127431894796466, 11.49999999999999645 ) ) ;
#69306=CARTESIAN_POINT ( 'NONE',  ( 22.64978874513612439, 0.4204215919581203442, 11.49999999999998934 ) ) ;
#69308=CARTESIAN_POINT ( 'NONE',  ( -27.75922577455652984, -24.80591230451047480, 7.602030938097199098 ) ) ;
#69309=EDGE_LOOP ( 'NONE', ( #98730, #87101, #65170, #85979 ) ) ;
#69310=ADVANCED_FACE ( 'NONE', ( #6719 ), #36678, .F. ) ;
#69311=ORIENTED_EDGE ( 'NONE', *, *, #52545, .T. ) ;
#69312=CARTESIAN_POINT ( 'NONE',  ( -68.22287095715007865, -23.47596703998600631, 11.44779298504227860 ) ) ;
#69314=CARTESIAN_POINT ( 'NONE',  ( -14.78635263257777233, 13.65558988533819473, -1.500000000000002220 ) ) ;
#69315=DIRECTION ( 'NONE',  ( 0.000000000000000000, -2.173523156925980399E-06, 0.9999999999976378895 ) ) ;
#69316=EDGE_LOOP ( 'NONE', ( #98045, #6412, #45748, #50003 ) ) ;
#69318=CARTESIAN_POINT ( 'NONE',  ( -20.85237562250380350, -7.973873963886685345, -1.500000000000002220 ) ) ;
#69320=VERTEX_POINT ( 'NONE', #68631 ) ;
#69321=CARTESIAN_POINT ( 'NONE',  ( -101.3040450898205620, -25.25341214910569931, 6.746837293798033208 ) ) ;
#69322=FACE_OUTER_BOUND ( 'NONE', #40358, .T. ) ;
#69323=PLANE ( 'NONE',  #66876 ) ;
#69325=AXIS2_PLACEMENT_3D ( 'NONE', #80075, #87186, #71477 ) ;
#69326=FACE_OUTER_BOUND ( 'NONE', #72026, .T. ) ;
#69327=CARTESIAN_POINT ( 'NONE',  ( 4.865394487973861537, 18.91859722749940786, 11.49999999999998934 ) ) ;
#69328=DIRECTION ( 'NONE',  ( -1.000000000000000000, -3.773278334444167608E-23, -8.201307833595939069E-29 ) ) ;
#69329=CARTESIAN_POINT ( 'NONE',  ( -8.581294335678165908, -19.67629172487136557, -1.500000000000002220 ) ) ;
#69331=CARTESIAN_POINT ( 'NONE',  ( -46.58953762381671737, -23.47596703998600276, 11.44779298504227505 ) ) ;
#69332=CARTESIAN_POINT ( 'NONE',  ( -59.62287095715004881, -23.48783264082478794, -1.443836473390069042 ) ) ;
#69333=CARTESIAN_POINT ( 'NONE',  ( -80.62287095714998486, -24.51254535404255108, 9.355368623467654743 ) ) ;
#69334=CARTESIAN_POINT ( 'NONE',  ( 2.723195454624489642, 22.67993996152103620, -1.500000000000002220 ) ) ;
#69338=CARTESIAN_POINT ( 'NONE',  ( -124.5228709571500616, -24.64965694238575722, 8.947790433994191162 ) ) ;
#69339=DIRECTION ( 'NONE',  ( 0.000000000000000000, 0.9999999999976377785, 2.173523156925979975E-06 ) ) ;
#69340=CARTESIAN_POINT ( 'NONE',  ( -6.099057486122481997, -19.05896565686126110, 11.49999999999999645 ) ) ;
#69341=CARTESIAN_POINT ( 'NONE',  ( -79.34156256387794315, -25.26612463273757925, 4.917719406326733100 ) ) ;
#69342=CARTESIAN_POINT ( 'NONE',  ( -111.5228709571500616, -23.47593901973090524, -1.443836447538996204 ) ) ;
#69345=B_SPLINE_CURVE_WITH_KNOTS ( 'NONE', 3,
 ( #36417, #43542, #13068, #51147, #35919, #44031 ),
 .UNSPECIFIED., .F., .F.,
 ( 4, 2, 4 ),
 ( 0.000000000000000000, 0.001380901958385387894, 0.002761803916770775788 ),
 .UNSPECIFIED. ) ;
#69346=CARTESIAN_POINT ( 'NONE',  ( -108.6228709571500559, -24.64898659630368627, 1.056161002820831474 ) ) ;
#69347=ORIENTED_EDGE ( 'NONE', *, *, #44090, .T. ) ;
#69348=CARTESIAN_POINT ( 'NONE',  ( -83.52287095715006160, -23.48786465467241769, 11.44779295918254469 ) ) ;
#69350=CARTESIAN_POINT ( 'NONE',  ( 21.56942612084361599, 2.798134137018522427, 11.49999999999998934 ) ) ;
#69351=EDGE_CURVE ( 'NONE', #62329, #80499, #26433, .T. ) ;
#69353=CARTESIAN_POINT ( 'NONE',  ( 0.9049686737998731134, -19.58615294826029540, -1.500000000000002220 ) ) ;
#69356=CARTESIAN_POINT ( 'NONE',  ( -40.70683750969132575, -25.18823549857387789, 3.317374228038964645 ) ) ;
#69358=CARTESIAN_POINT ( 'NONE',  ( -91.55173743107893358, -24.15620529776628445, 10.23563542870660292 ) ) ;
#69359=DIRECTION ( 'NONE',  ( -3.773278334453079030E-23, 0.9999999999976377785, 2.173523156925979128E-06 ) ) ;
#69360=CARTESIAN_POINT ( 'NONE',  ( -4.979992623568794130, 19.86841884474198494, 11.49999999999999645 ) ) ;
#69362=CARTESIAN_POINT ( 'NONE',  ( -46.52287095715004028, -24.66019654487199375, 8.947790411086122830 ) ) ;
#69364=CARTESIAN_POINT ( 'NONE',  ( -100.0631793594960044, -25.31296428244992569, 4.632688900756619432 ) ) ;
#69366=CARTESIAN_POINT ( 'NONE',  ( -125.5562614031464932, -23.85049219812686871, 10.88485053497526778 ) ) ;
#69370=CARTESIAN_POINT ( 'NONE',  ( -38.52287095715006870, -24.64965694238406613, 8.947790433994205372 ) ) ;
#69372=CARTESIAN_POINT ( 'NONE',  ( 3.314627170985911420, 22.80399709308638023, 11.49999999999999645 ) ) ;
#69373=CARTESIAN_POINT ( 'NONE',  ( -6.082769120682566921, -21.99330073093985405, 11.49999999999998934 ) ) ;
#69374=CARTESIAN_POINT ( 'NONE',  ( -104.5228709571501184, -24.33832256527049154, 0.1851278514138610942 ) ) ;
#69375=B_SPLINE_SURFACE_WITH_KNOTS ( 'NONE', 3, 3, ( 
 ( #87181, #24285, #1961, #25781 ),
 ( #10057, #63874, #17669, #56256 ),
 ( #40007, #39004, #70967, #48642 ),
 ( #71973, #1458, #41019, #78049 ),
 ( #24771, #2454, #8563, #56757 ),
 ( #69957, #55753, #442, #86680 ),
 ( #48133, #34899, #72468, #72969 ) ),
 .UNSPECIFIED., .F., .F., .F.,
 ( 4, 3, 4 ),
 ( 4, 4 ),
 ( 0.0004766839783817961962, 0.1029713700210893035, 0.2054660560637968092 ),
 ( 0.7896948821346888581, 0.7910719704583279999 ),
 .UNSPECIFIED. ) ;
#69376=CARTESIAN_POINT ( 'NONE',  ( -75.52287095715007581, -23.84081130425355965, 10.88220057483160907 ) ) ;
#69378=CARTESIAN_POINT ( 'NONE',  ( -17.93832129671990572, 13.47109510200611560, 11.49999999999999645 ) ) ;
#69381=CARTESIAN_POINT ( 'NONE',  ( -43.56913326832147959, -23.48783264082478084, -1.443836473390076369 ) ) ;
#69382=CARTESIAN_POINT ( 'NONE',  ( -20.07106029494397248, -8.819774368769808248, -1.500000000000002220 ) ) ;
#69383=ADVANCED_FACE ( 'NONE', ( #94962 ), #48300, .T. ) ;
#69384=CARTESIAN_POINT ( 'NONE',  ( -113.5228709571500616, -23.96127896941632685, -0.6493128931037960294 ) ) ;
#69385=CARTESIAN_POINT ( 'NONE',  ( -87.54530861272236564, -24.51419770103156281, 9.386484678747175181 ) ) ;
#69386=CARTESIAN_POINT ( 'NONE',  ( -114.6228709571500559, -23.47593901973091235, -1.443836447538999312 ) ) ;
#69387=ADVANCED_FACE ( 'NONE', ( #70125 ), #40181, .F. ) ;
#69388=CARTESIAN_POINT ( 'NONE',  ( -49.21454750704995007, -25.12863070112381791, 7.069183623698430452 ) ) ;
#69390=VERTEX_POINT ( 'NONE', #25451 ) ;
#69391=CARTESIAN_POINT ( 'NONE',  ( -0.3173379506236611580, 20.48240526196808631, -1.500000000000002220 ) ) ;
#69392=ORIENTED_EDGE ( 'NONE', *, *, #62222, .T. ) ;
#69394=VERTEX_POINT ( 'NONE', #31558 ) ;
#69396=CARTESIAN_POINT ( 'NONE',  ( -21.10450430117995424, 9.351148110661185342, -1.500000000000002220 ) ) ;
#69397=CARTESIAN_POINT ( 'NONE',  ( -102.5562042904833930, -24.66019654487199730, 8.947790411086122830 ) ) ;
#69398=EDGE_CURVE ( 'NONE', #82785, #74711, #16707, .T. ) ;
#69399=CARTESIAN_POINT ( 'NONE',  ( -15.58492919356500650, -12.95507736684500699, -1.500000000000002220 ) ) ;
#69402=AXIS2_PLACEMENT_3D ( 'NONE', #18194, #16305, #85823 ) ;
#69404=EDGE_CURVE ( 'NONE', #3899, #50986, #71170, .T. ) ;
#69406=CARTESIAN_POINT ( 'NONE',  ( -28.52287095715005449, -24.34211201941327474, 9.387659967996357935 ) ) ;
#69407=CARTESIAN_POINT ( 'NONE',  ( -70.54094150479154735, -24.63355581998385091, 0.9682620441943861067 ) ) ;
#69408=CARTESIAN_POINT ( 'NONE',  ( 4.199879391047538491, -21.09745483596041282, 11.49999999999999645 ) ) ;
#69409=EDGE_LOOP ( 'NONE', ( #32993, #74637, #77594, #39182 ) ) ;
#69410=CARTESIAN_POINT ( 'NONE',  ( -75.64173089025919694, -24.15503026093913874, -0.2815557561904522554 ) ) ;
#69411=CARTESIAN_POINT ( 'NONE',  ( -61.49449328950704086, -24.51419770103157347, 9.386484678747178734 ) ) ;
#69412=ORIENTED_EDGE ( 'NONE', *, *, #80061, .T. ) ;
#69413=CARTESIAN_POINT ( 'NONE',  ( 10.87737074370964407, 17.65887017642603851, 11.49999999999998934 ) ) ;
#69415=FACE_OUTER_BOUND ( 'NONE', #44575, .T. ) ;
#69416=ORIENTED_EDGE ( 'NONE', *, *, #70022, .T. ) ;
#69418=EDGE_LOOP ( 'NONE', ( #83649, #24583, #7276, #32140 ) ) ;
#69421=VECTOR ( 'NONE', #21304, 1000.000000000000114 ) ;
#69422=CARTESIAN_POINT ( 'NONE',  ( -42.54639151317959289, -24.15620529776627734, 10.23563542870661358 ) ) ;
#69423=CARTESIAN_POINT ( 'NONE',  ( -65.48373801871647970, -25.00158670708910691, 2.256160236439222366 ) ) ;
#69424=CARTESIAN_POINT ( 'NONE',  ( -8.017166757594178961, 20.41873492177044724, 11.49999999999999645 ) ) ;
#69426=CARTESIAN_POINT ( 'NONE',  ( 8.566404662457630437, 20.85315857434707709, 11.49999999999998934 ) ) ;
#69427=CARTESIAN_POINT ( 'NONE',  ( 8.737904895026865404, 19.08465823478955414, 11.49999999999998934 ) ) ;
#69428=CARTESIAN_POINT ( 'NONE',  ( -89.62287095715005592, -23.72747288104470442, -1.053458166803225682 ) ) ;
#69429=CARTESIAN_POINT ( 'NONE',  ( -100.6228709571500559, -29.50247984919015209, -1.443849546365050029 ) ) ;
#69432=ORIENTED_EDGE ( 'NONE', *, *, #9701, .F. ) ;
#69434=CARTESIAN_POINT ( 'NONE',  ( -80.62287095715005592, -24.14321612903114911, -0.2833117244521584643 ) ) ;
#69435=CARTESIAN_POINT ( 'NONE',  ( 2.564635614221720594, -21.35862533600356983, -1.500000000000002220 ) ) ;
#69437=B_SPLINE_CURVE_WITH_KNOTS ( 'NONE', 3,
 ( #89500, #6253, #13860, #59560 ),
 .UNSPECIFIED., .F., .F.,
 ( 4, 4 ),
 ( 0.000000000000000000, 9.999999999998206125E-05 ),
 .UNSPECIFIED. ) ;
#69438=CARTESIAN_POINT ( 'NONE',  ( -113.6228709571500701, -23.72773821059536559, 11.05748984161097503 ) ) ;
#69439=ORIENTED_EDGE ( 'NONE', *, *, #54752, .F. ) ;
#69440=CARTESIAN_POINT ( 'NONE',  ( -21.09505027744838657, -1.104435277493458045, -1.500000000000002220 ) ) ;
#69442=CARTESIAN_POINT ( 'NONE',  ( -58.86102183801504140, -25.14083923594471059, 2.947789366366678987 ) ) ;
#69443=CARTESIAN_POINT ( 'NONE',  ( -83.59538750566655096, -23.96169478059713143, 10.65365249895718058 ) ) ;
#69444=CARTESIAN_POINT ( 'NONE',  ( -119.5228709571500758, -29.50248528299804818, 1.056150453629045360 ) ) ;
#69446=CARTESIAN_POINT ( 'NONE',  ( -12.03526013704878039, -18.61824004984164560, -1.500000000000002220 ) ) ;
#69448=VERTEX_POINT ( 'NONE', #62520 ) ;
#69449=CARTESIAN_POINT ( 'NONE',  ( -51.85051548866884019, -25.24860163112497347, 5.725681047314564509 ) ) ;
#69451=CARTESIAN_POINT ( 'NONE',  ( 2.021814659504407579E-13, -19.30000000000000426, 11.49999999999999645 ) ) ;
#69452=CARTESIAN_POINT ( 'NONE',  ( -100.5838749402658294, -25.00158670708910691, 2.256160236439218369 ) ) ;
#69453=CARTESIAN_POINT ( 'NONE',  ( -8.858824863812619910, -17.32749669425128047, 11.49999999999998934 ) ) ;
#69454=CARTESIAN_POINT ( 'NONE',  ( -21.34312709018487553, 1.176582458498846462, 11.49999999999998934 ) ) ;
#69458=CARTESIAN_POINT ( 'NONE',  ( -101.3738023147422780, -25.18440161649941800, 3.986250810164079450 ) ) ;
#69459=CARTESIAN_POINT ( 'NONE',  ( 21.55457256799317278, 7.124301260279622738, -1.500000000000002220 ) ) ;
#69461=B_SPLINE_SURFACE_WITH_KNOTS ( 'NONE', 3, 3, ( 
 ( #42312, #10840, #64656, #26057 ),
 ( #87965, #18446, #41804, #34180 ),
 ( #65156, #76211, #68123, #29544 ),
 ( #21919, #91945, #7201, #52395 ),
 ( #5714, #6705, #38150, #83834 ),
 ( #13313, #44292, #52898, #82338 ),
 ( #74716, #99044, #69104, #60521 ),
 ( #5218, #14809, #75709, #45285 ),
 ( #45776, #30544, #36174, #91436 ),
 ( #22415, #67140, #75221, #14311 ) ),
 .UNSPECIFIED., .F., .F., .F.,
 ( 4, 3, 3, 4 ),
 ( 4, 4 ),
 ( 0.7022005934544806038, 0.7765311282028795059, 0.8508616629512784080, 0.9995227324480763231 ),
 ( 0.4995542859879725239, 0.5008647382424362693 ),
 .UNSPECIFIED. ) ;
#69462=CARTESIAN_POINT ( 'NONE',  ( -98.62287095715007013, -23.47596703998600631, 11.44779298504227860 ) ) ;
#69463=CARTESIAN_POINT ( 'NONE',  ( -115.6228709571500559, -29.50248528299804818, 1.056150453629045360 ) ) ;
#69464=CARTESIAN_POINT ( 'NONE',  ( 14.04693994163893578, -13.95676237773968609, 11.49999999999999645 ) ) ;
#69465=VECTOR ( 'NONE', #49947, 1000.000000000000114 ) ;
#69466=CARTESIAN_POINT ( 'NONE',  ( -68.93918693012690824, -25.24795196732124936, 6.184868460502651821 ) ) ;
#69467=ORIENTED_EDGE ( 'NONE', *, *, #11334, .F. ) ;
#69468=DIRECTION ( 'NONE',  ( 0.000000000000000000, 2.173523156925980399E-06, -0.9999999999976378895 ) ) ;
#69472=CARTESIAN_POINT ( 'NONE',  ( 18.46943957830784555, -11.30625484363265265, -1.500000000000002220 ) ) ;
#69473=EDGE_CURVE ( 'NONE', #95938, #17861, #53025, .T. ) ;
#69474=CARTESIAN_POINT ( 'NONE',  ( -66.62287095715005592, -24.65952944569304606, 1.056160979905696573 ) ) ;
#69475=AXIS2_PLACEMENT_3D ( 'NONE', #22709, #13609, #98344 ) ;
#69476=CARTESIAN_POINT ( 'NONE',  ( -15.52061920455031618, -11.66286593722069931, -1.500000000000002220 ) ) ;
#69478=CARTESIAN_POINT ( 'NONE',  ( -114.5228709571500616, -24.64965694238408034, 8.947790433994192938 ) ) ;
#69479=CARTESIAN_POINT ( 'NONE',  ( -55.64120953861098684, -24.40133493613049964, 9.663955038902800609 ) ) ;
#69480=CARTESIAN_POINT ( 'NONE',  ( 16.46483878678964174, 11.07114234313464252, -1.500000000000002220 ) ) ;
#69481=ORIENTED_EDGE ( 'NONE', *, *, #89659, .F. ) ;
#69483=AXIS2_PLACEMENT_3D ( 'NONE', #50161, #81098, #42557 ) ;
#69485=CARTESIAN_POINT ( 'NONE',  ( -3.780122020211411193, 19.97858748211865532, 11.49999999999999645 ) ) ;
#69486=CARTESIAN_POINT ( 'NONE',  ( -80.53777470234541624, -24.92564183028979130, 1.928384488918253536 ) ) ;
#69489=B_SPLINE_CURVE_WITH_KNOTS ( 'NONE', 3,
 ( #74065, #42134, #43615, #81170 ),
 .UNSPECIFIED., .F., .F.,
 ( 4, 4 ),
 ( 0.3307361706037946214, 0.3397426018759102107 ),
 .UNSPECIFIED. ) ;
#69490=CARTESIAN_POINT ( 'NONE',  ( -102.6251301713998458, -24.51419770103155926, 9.386484678747178734 ) ) ;
#69491=CARTESIAN_POINT ( 'NONE',  ( -116.4728709571500502, -25.40675428744130926, 5.000950440044785061 ) ) ;
#69492=CARTESIAN_POINT ( 'NONE',  ( -58.87764846857956513, -25.14083923594470704, 2.947789366366647901 ) ) ;
#69493=VECTOR ( 'NONE', #27700, 1000.000000000000114 ) ;
#69494=CARTESIAN_POINT ( 'NONE',  ( -40.59314885895794589, -24.40133493613049609, 9.663955038902802386 ) ) ;
#69496=CARTESIAN_POINT ( 'NONE',  ( 18.99975792849237877, 6.539580213093530325, -1.500000000000002220 ) ) ;
#69498=CARTESIAN_POINT ( 'NONE',  ( -95.62287095715005592, -24.99132157543084531, 2.256160258750667502 ) ) ;
#69499=ORIENTED_EDGE ( 'NONE', *, *, #14760, .F. ) ;
#69500=CARTESIAN_POINT ( 'NONE',  ( -36.52287095715007581, -23.94994826722564696, -0.6494450866342753592 ) ) ;
#69501=CARTESIAN_POINT ( 'NONE',  ( 12.66508800429495629, 19.07499079241581086, 11.49999999999999645 ) ) ;
#69502=CARTESIAN_POINT ( 'NONE',  ( -22.67762270672801250, 1.536325718666671225, -1.500000000000002220 ) ) ;
#69504=CARTESIAN_POINT ( 'NONE',  ( -109.6228709571500275, -23.96127896941632685, -0.6493128931037813745 ) ) ;
#69505=CARTESIAN_POINT ( 'NONE',  ( -126.5228709571500616, -23.96177878511310055, 10.65340807706329507 ) ) ;
#69506=CARTESIAN_POINT ( 'NONE',  ( -38.53898738578955374, -24.35071581493542325, 9.817618358456030592 ) ) ;
#69509=CARTESIAN_POINT ( 'NONE',  ( -84.62287095715007013, -23.48786465467241769, 11.44779295918254469 ) ) ;
#69512=LINE ( 'NONE', #7602, #79317 ) ;
#69514=CARTESIAN_POINT ( 'NONE',  ( 19.80222353126469415, -4.898785079568316547, -1.500000000000002220 ) ) ;
#69516=CARTESIAN_POINT ( 'NONE',  ( 16.94363762160741516, 15.55198921429254533, 11.49999999999998934 ) ) ;
#69517=ADVANCED_FACE ( 'NONE', ( #72642 ), #96828, .T. ) ;
#69518=CARTESIAN_POINT ( 'NONE',  ( -45.52287095715004739, -24.51163499207175889, 0.6490370598554249248 ) ) ;
#69520=CARTESIAN_POINT ( 'NONE',  ( -108.6294922829741267, -23.96169478059714208, 10.65365249895716993 ) ) ;
#69521=EDGE_CURVE ( 'NONE', #60463, #30073, #90571, .T. ) ;
#69523=EDGE_CURVE ( 'NONE', #31069, #63463, #90351, .T. ) ;
#69524=B_SPLINE_CURVE_WITH_KNOTS ( 'NONE', 3,
 ( #45614, #7041, #36993, #13143 ),
 .UNSPECIFIED., .F., .F.,
 ( 4, 4 ),
 ( 0.000000000000000000, 9.999999999996123101E-05 ),
 .UNSPECIFIED. ) ;
#69525=CARTESIAN_POINT ( 'NONE',  ( -51.49047045075048601, -24.51419770103156637, 9.386484678747175181 ) ) ;
#69526=CARTESIAN_POINT ( 'NONE',  ( 14.70648301983428397, -15.34743991077593250, 11.49999999999999645 ) ) ;
#69527=EDGE_LOOP ( 'NONE', ( #23959, #31707, #86159, #31354 ) ) ;
#69529=CARTESIAN_POINT ( 'NONE',  ( -0.8134642310582372859, 22.17477653155656725, 11.49999999999998934 ) ) ;
#69530=CARTESIAN_POINT ( 'NONE',  ( 1.582324178664715975, -20.54890914157308401, 11.49999999999998934 ) ) ;
#69531=ORIENTED_EDGE ( 'NONE', *, *, #71496, .F. ) ;
#69533=FACE_OUTER_BOUND ( 'NONE', #61607, .T. ) ;
#69536=VERTEX_POINT ( 'NONE', #43679 ) ;
#69538=CARTESIAN_POINT ( 'NONE',  ( -91.59442398169517219, -23.96119346886881019, -0.6495511937832073590 ) ) ;
#69540=ORIENTED_EDGE ( 'NONE', *, *, #61396, .T. ) ;
#69541=CARTESIAN_POINT ( 'NONE',  ( -39.52287095715006870, -23.72773821059535848, 11.05748984161097681 ) ) ;
#69542=B_SPLINE_CURVE_WITH_KNOTS ( 'NONE', 3,
 ( #83438, #44903, #75825, #6324, #37280, #16928 ),
 .UNSPECIFIED., .F., .F.,
 ( 4, 2, 4 ),
 ( 0.000000000000000000, 0.001380901958385386376, 0.002761803916770772752 ),
 .UNSPECIFIED. ) ;
#69543=DIRECTION ( 'NONE',  ( 0.000000000000000000, 0.9999999999976377785, 2.173523156925979975E-06 ) ) ;
#69544=CARTESIAN_POINT ( 'NONE',  ( 8.324980675869593227, 19.10421180063631752, -1.500000000000002220 ) ) ;
#69545=CARTESIAN_POINT ( 'NONE',  ( -20.93004649427559016, -6.003493321846349318, 11.49999999999999645 ) ) ;
#69547=CARTESIAN_POINT ( 'NONE',  ( -99.67810188082559364, -25.06709179204377591, 7.399672078504718975 ) ) ;
#69548=CARTESIAN_POINT ( 'NONE',  ( 11.54466316424315231, -19.26756404802103972, 11.49999999999998934 ) ) ;
#69549=AXIS2_PLACEMENT_3D ( 'NONE', #61564, #16363, #69156 ) ;
#69550=FACE_OUTER_BOUND ( 'NONE', #9004, .T. ) ;
#69553=CARTESIAN_POINT ( 'NONE',  ( -51.61997180002916963, -25.22394202344478131, 3.594056534852918983 ) ) ;
#69555=AXIS2_PLACEMENT_3D ( 'NONE', #89351, #19818, #59397 ) ;
#69558=B_SPLINE_CURVE_WITH_KNOTS ( 'NONE', 3,
 ( #74022, #90241, #66433, #28336, #59296, #4516 ),
 .UNSPECIFIED., .F., .F.,
 ( 4, 2, 4 ),
 ( 0.000000000000000000, 0.001380901958385388545, 0.002761803916770777089 ),
 .UNSPECIFIED. ) ;
#69559=CARTESIAN_POINT ( 'NONE',  ( 15.73328655151706101, -14.44092690703295467, -1.500000000000002220 ) ) ;
#69560=ORIENTED_EDGE ( 'NONE', *, *, #61307, .T. ) ;
#69561=CARTESIAN_POINT ( 'NONE',  ( 11.68726034403320746, 17.49698133428071145, -1.500000000000002220 ) ) ;
#69562=CARTESIAN_POINT ( 'NONE',  ( -30.45988033841292975, -25.30656340722048014, 3.857144010898052588 ) ) ;
#69564=CARTESIAN_POINT ( 'NONE',  ( -111.3419982013945173, -25.27993372741254063, 4.063003188440275082 ) ) ;
#69565=CARTESIAN_POINT ( 'NONE',  ( -49.85473837878901548, -25.05837338253707713, 7.491380643917580073 ) ) ;
#69566=CARTESIAN_POINT ( 'NONE',  ( -21.26704322615652032, -5.532269525099344776, -1.500000000000002220 ) ) ;
#69567=CARTESIAN_POINT ( 'NONE',  ( -52.62287095715004881, -23.72747288104442021, -1.053458166803663110 ) ) ;
#69568=EDGE_LOOP ( 'NONE', ( #80805, #75912, #67826, #24232 ) ) ;
#69570=B_SPLINE_CURVE_WITH_KNOTS ( 'NONE', 3,
 ( #97023, #57485, #19887, #66606 ),
 .UNSPECIFIED., .F., .F.,
 ( 4, 4 ),
 ( 1.785902608152995868E-11, 0.002468655811832971662 ),
 .UNSPECIFIED. ) ;
#69571=CARTESIAN_POINT ( 'NONE',  ( -127.5895376238167245, -23.47596703998600631, 11.44779298504227683 ) ) ;
#69572=CARTESIAN_POINT ( 'NONE',  ( 7.204507412156021751, -19.57454612608841771, 11.49999999999999645 ) ) ;
#69574=CARTESIAN_POINT ( 'NONE',  ( -111.6228709571500701, -23.48786465467241769, 11.44779295918254114 ) ) ;
#69575=DIRECTION ( 'NONE',  ( -3.773278334453079030E-23, 0.9999999999976377785, 2.173523156925979128E-06 ) ) ;
#69576=CARTESIAN_POINT ( 'NONE',  ( 9.569808575145499319, 19.01914523534739132, -1.500000000000002220 ) ) ;
#69581=CARTESIAN_POINT ( 'NONE',  ( -21.69688529672534827, 6.072505851105969299, -1.500000000000002220 ) ) ;
#69586=ADVANCED_FACE ( 'NONE', ( #52794 ), #67523, .F. ) ;
#69587=CARTESIAN_POINT ( 'NONE',  ( -80.35919894935767616, -25.29542306156489673, 4.505481338088394239 ) ) ;
#69588=CARTESIAN_POINT ( 'NONE',  ( 17.63768857353127828, -8.544740250177758512, 11.49999999999999645 ) ) ;
#69591=VERTEX_POINT ( 'NONE', #14714 ) ;
#69593=CARTESIAN_POINT ( 'NONE',  ( -50.58953762381671027, -23.48783264082478084, -1.443836473390070596 ) ) ;
#69594=CARTESIAN_POINT ( 'NONE',  ( -108.5895376238167245, -24.66019654487199730, 8.947790411086135265 ) ) ;
#69595=CARTESIAN_POINT ( 'NONE',  ( -91.96486695379628884, -25.25787539255926362, 3.590294762828090125 ) ) ;
#69597=ADVANCED_FACE ( 'NONE', ( #76109 ), #6611, .T. ) ;
#69598=CARTESIAN_POINT ( 'NONE',  ( 17.76913753361954562, 8.601950719843506121, -1.500000000000002220 ) ) ;
#69599=EDGE_LOOP ( 'NONE', ( #44587, #21326, #4534, #62273 ) ) ;
#69600=EDGE_CURVE ( 'NONE', #44562, #51996, #96687, .T. ) ;
#69601=CARTESIAN_POINT ( 'NONE',  ( -109.8525198310536126, -25.20967124336913301, 3.399964862456664072 ) ) ;
#69603=ORIENTED_EDGE ( 'NONE', *, *, #38903, .F. ) ;
#69604=CARTESIAN_POINT ( 'NONE',  ( -46.52287095715007581, -23.47593901973090524, -1.443836447538997314 ) ) ;
#69605=CARTESIAN_POINT ( 'NONE',  ( -107.6228709571500701, -23.48783264082479150, -1.443836473390060382 ) ) ;
#69607=LINE ( 'NONE', #15301, #94694 ) ;
#69610=CARTESIAN_POINT ( 'NONE',  ( -56.62287095715005592, -24.65952944569304250, 1.056160979905693464 ) ) ;
#69612=CARTESIAN_POINT ( 'NONE',  ( -19.95465934538571062, -0.7993260556091378310, 11.49999999999998934 ) ) ;
#69615=CARTESIAN_POINT ( 'NONE',  ( -45.63952611995537723, -24.52399227489127043, 9.353111116836528183 ) ) ;
#69618=ADVANCED_FACE ( 'NONE', ( #92339 ), #6108, .F. ) ;
#69620=FACE_OUTER_BOUND ( 'NONE', #67912, .T. ) ;
#69621=CARTESIAN_POINT ( 'NONE',  ( -109.3592350823140720, -25.18430345422392236, 4.175498078355194487 ) ) ;
#69623=CARTESIAN_POINT ( 'NONE',  ( -100.5228709571500616, -23.48786465467242479, 11.44779295918254114 ) ) ;
#69625=CARTESIAN_POINT ( 'NONE',  ( -97.52287095715006160, -24.65952944569304606, 1.056160979905702346 ) ) ;
#69626=CARTESIAN_POINT ( 'NONE',  ( -83.54166051555876038, -24.65952944569304606, 1.056160979905700126 ) ) ;
#69630=ORIENTED_EDGE ( 'NONE', *, *, #86216, .T. ) ;
#69631=B_SPLINE_CURVE_WITH_KNOTS ( 'NONE', 3,
 ( #100000, #92404, #29012, #59982 ),
 .UNSPECIFIED., .F., .F.,
 ( 4, 4 ),
 ( 1.387778780781445521E-17, 9.999999999997510880E-05 ),
 .UNSPECIFIED. ) ;
#69632=CARTESIAN_POINT ( 'NONE',  ( -14.64122064730360862, 14.02963135428074004, -1.500000000000002220 ) ) ;
#69634=CARTESIAN_POINT ( 'NONE',  ( -90.52287095715004739, -23.84047902841604838, -0.8780736468305390119 ) ) ;
#69637=CARTESIAN_POINT ( 'NONE',  ( -95.52287095715006160, -23.47596703998600631, 11.44779298504228215 ) ) ;
#69638=CARTESIAN_POINT ( 'NONE',  ( 4.282148337517553749, -19.64591042314588165, -1.500000000000002220 ) ) ;
#69639=CARTESIAN_POINT ( 'NONE',  ( -4.359323203648655998, -20.60729432550360585, 11.49999999999999645 ) ) ;
#69640=CARTESIAN_POINT ( 'NONE',  ( 12.17348956504948987, -18.45705692928949659, 11.49999999999998934 ) ) ;
#69642=CARTESIAN_POINT ( 'NONE',  ( -19.38928925021375349, 6.733644070511561885, -1.500000000000002220 ) ) ;
#69643=FACE_OUTER_BOUND ( 'NONE', #97809, .T. ) ;
#69644=CARTESIAN_POINT ( 'NONE',  ( -53.62287095715004881, -24.65952944569303895, 1.056160979905692576 ) ) ;
#69646=PLANE ( 'NONE',  #8737 ) ;
#69648=LINE ( 'NONE', #1641, #13862 ) ;
#69649=B_SPLINE_SURFACE_WITH_KNOTS ( 'NONE', 3, 3, ( 
 ( #9105, #25831, #31947, #63419 ),
 ( #17216, #95344, #48182, #2507 ),
 ( #71521, #2007, #56806, #49193 ),
 ( #59280, #88241, #4002, #42076 ),
 ( #43064, #44055, #65427, #57310 ),
 ( #26336, #18707, #4505, #5488 ),
 ( #90229, #57796, #20702, #49687 ) ),
 .UNSPECIFIED., .F., .F., .F.,
 ( 4, 3, 4 ),
 ( 4, 4 ),
 ( 0.0004766839783818023761, 0.1029713700210893174, 0.2054660560637968370 ),
 ( 0.7196770707996874572, 0.7210218530338301512 ),
 .UNSPECIFIED. ) ;
#69652=ORIENTED_EDGE ( 'NONE', *, *, #78456, .F. ) ;
#69654=CARTESIAN_POINT ( 'NONE',  ( -118.6228709571500417, -23.72747288104441665, -1.053458166803660667 ) ) ;
#69655=CARTESIAN_POINT ( 'NONE',  ( -63.62287095715003460, -23.48783264082478084, -1.443836473390069042 ) ) ;
#69656=CARTESIAN_POINT ( 'NONE',  ( -68.64046488457991302, -23.96169478059712787, 10.65365249895718414 ) ) ;
#69657=CARTESIAN_POINT ( 'NONE',  ( 9.220172233967117492, 18.46515239161685784, -1.500000000000002220 ) ) ;
#69658=CARTESIAN_POINT ( 'NONE',  ( 20.63042821663210091, 6.393326493806346100, 11.49999999999999645 ) ) ;
#69660=CARTESIAN_POINT ( 'NONE',  ( -83.62287095715009855, -24.50216790748099527, 0.6166512839513712541 ) ) ;
#69662=CARTESIAN_POINT ( 'NONE',  ( -6.430504157862594994, -21.42354456762059201, 11.49999999999998934 ) ) ;
#69663=CARTESIAN_POINT ( 'NONE',  ( -71.52287095715007581, -23.96127896941631619, -0.6493128931038050222 ) ) ;
#69664=CARTESIAN_POINT ( 'NONE',  ( -84.54457827582588436, -24.51314013834316441, 0.6176544820404183955 ) ) ;
#69665=ORIENTED_EDGE ( 'NONE', *, *, #33976, .F. ) ;
#69667=CARTESIAN_POINT ( 'NONE',  ( -62.52287095715006160, -24.65952944569304606, 1.056160979905695463 ) ) ;
#69668=CARTESIAN_POINT ( 'NONE',  ( -115.5228709571500474, -23.47593901973090524, -1.443836447538996204 ) ) ;
#69669=CARTESIAN_POINT ( 'NONE',  ( -16.13976855045889636, 13.32451261336467496, 11.49999999999998934 ) ) ;
#69670=ORIENTED_EDGE ( 'NONE', *, *, #81277, .F. ) ;
#69672=CARTESIAN_POINT ( 'NONE',  ( -98.62287095715007013, -24.33832256526968862, 0.1851278514119928387 ) ) ;
#69673=ORIENTED_EDGE ( 'NONE', *, *, #91901, .F. ) ;
#69674=CARTESIAN_POINT ( 'NONE',  ( -50.62287095715005592, -23.47596703998600631, 11.44779298504227505 ) ) ;
#69675=CARTESIAN_POINT ( 'NONE',  ( 10.98566517548414012, -18.08203305749968592, -1.500000000000002220 ) ) ;
#69678=CARTESIAN_POINT ( 'NONE',  ( 18.19902423439809525, 11.99547645517801442, 11.49999999999998934 ) ) ;
#69681=LINE ( 'NONE', #37724, #69230 ) ;
#69682=CARTESIAN_POINT ( 'NONE',  ( 8.287826148123016878, -20.17477452812186201, -1.500000000000002220 ) ) ;
#69684=VERTEX_POINT ( 'NONE', #67037 ) ;
#69686=CARTESIAN_POINT ( 'NONE',  ( -117.5228709571500758, -24.33832256527049509, 0.1851278514138643139 ) ) ;
#69687=ORIENTED_EDGE ( 'NONE', *, *, #94900, .F. ) ;
#69688=VECTOR ( 'NONE', #62458, 1000.000000000000114 ) ;
#69689=B_SPLINE_CURVE_WITH_KNOTS ( 'NONE', 3,
 ( #99220, #7373, #69284, #6388 ),
 .UNSPECIFIED., .F., .F.,
 ( 4, 4 ),
 ( 0.000000000000000000, 0.0001002978978731668673 ),
 .UNSPECIFIED. ) ;
#69692=VERTEX_POINT ( 'NONE', #28439 ) ;
#69694=CARTESIAN_POINT ( 'NONE',  ( -125.6228709571500559, -23.47596703998600631, 11.44779298504227860 ) ) ;
#69695=CARTESIAN_POINT ( 'NONE',  ( 16.91677535067316995, -12.78530099663392505, -1.500000000000002220 ) ) ;
#69696=CARTESIAN_POINT ( 'NONE',  ( -94.51007522493627278, -24.34968618360933945, 0.1864209137778860548 ) ) ;
#69697=CARTESIAN_POINT ( 'NONE',  ( -79.25918010276897974, -25.27791844016729073, 6.969965416359520383 ) ) ;
#69701=CARTESIAN_POINT ( 'NONE',  ( 17.07123823605233781, 9.195568589125342029, 11.49999999999998934 ) ) ;
#69702=EDGE_CURVE ( 'NONE', #46879, #42461, #76006, .T. ) ;
#69703=CARTESIAN_POINT ( 'NONE',  ( -70.35895856474229504, -25.31161946917133321, 5.313173610579343453 ) ) ;
#69705=ADVANCED_FACE ( 'NONE', ( #98951 ), #75117, .F. ) ;
#69706=CARTESIAN_POINT ( 'NONE',  ( -16.21482014894483470, 10.69450053600103345, 11.49999999999999645 ) ) ;
#69707=CARTESIAN_POINT ( 'NONE',  ( -108.5228709571500616, -23.47596703998600631, 11.44779298504228038 ) ) ;
#69708=CARTESIAN_POINT ( 'NONE',  ( -111.6228709571500559, -24.65952944569304606, 1.056160979905703901 ) ) ;
#69709=VERTEX_POINT ( 'NONE', #56691 ) ;
#69710=ADVANCED_FACE ( 'NONE', ( #62925 ), #93847, .F. ) ;
#69713=EDGE_CURVE ( 'NONE', #98447, #7140, #9531, .T. ) ;
#69714=DIRECTION ( 'NONE',  ( -3.773278334453079030E-23, 0.9999999999976377785, 2.173523156925979128E-06 ) ) ;
#69715=CARTESIAN_POINT ( 'NONE',  ( -55.62287095715007013, -24.52232992886360563, 0.6492154411906059241 ) ) ;
#69716=CARTESIAN_POINT ( 'NONE',  ( -6.723608784814384620, 18.44229941887336821, 11.49999999999998934 ) ) ;
#69717=B_SPLINE_CURVE_WITH_KNOTS ( 'NONE', 3,
 ( #13728, #91858, #30465, #7629, #90364, #53311, #22827, #38578, #99953, #28961, #84243, #18, #5626, #98966, #52811, #45696, #69027, #59420 ),
 .UNSPECIFIED., .F., .F.,
 ( 4, 2, 2, 2, 2, 2, 2, 2, 4 ),
 ( 0.000000000000000000, 0.0002722776847237221888, 0.0005445553694474455702, 0.0008168330541711689517, 0.001089110738894892442, 0.001361388423618615715, 0.001633666108342339204, 0.001905943793066062477, 0.002178221477789786184 ),
 .UNSPECIFIED. ) ;
#69719=EDGE_LOOP ( 'NONE', ( #28365, #55483, #72045, #54208 ) ) ;
#69720=CARTESIAN_POINT ( 'NONE',  ( -21.57561264457377348, 0.06291308125064201673, -1.500000000000002220 ) ) ;
#69721=CARTESIAN_POINT ( 'NONE',  ( -95.52287095715009002, -24.15516710230293995, 10.28746687063726029 ) ) ;
#69723=CARTESIAN_POINT ( 'NONE',  ( -74.52287095715007581, -29.50250243563736774, 8.947779886222143375 ) ) ;
#69724=CARTESIAN_POINT ( 'NONE',  ( -90.52287095715009002, -24.92604778743017846, 8.074972756849364330 ) ) ;
#69725=CARTESIAN_POINT ( 'NONE',  ( -10.12245940999746985, -20.73198382670940987, -1.500000000000002220 ) ) ;
#69727=CARTESIAN_POINT ( 'NONE',  ( -93.55798330475117552, -23.73766607897670511, -1.055555164236453569 ) ) ;
#69729=CARTESIAN_POINT ( 'NONE',  ( -41.26959558397307148, -25.08918874615346439, 7.338714959427068862 ) ) ;
#69731=CARTESIAN_POINT ( 'NONE',  ( -109.8541577975467192, -25.19951037986027131, 3.399436371649390498 ) ) ;
#69733=CARTESIAN_POINT ( 'NONE',  ( -114.5168350146848155, -24.35071581493544457, 9.817618358456016381 ) ) ;
#69734=CARTESIAN_POINT ( 'NONE',  ( 11.24879072547334324, 16.40116332625411033, 11.49999999999998934 ) ) ;
#69736=CARTESIAN_POINT ( 'NONE',  ( -7.013475202606065828, -18.52788797337992222, -1.500000000000002220 ) ) ;
#69738=LINE ( 'NONE', #219, #88962 ) ;
#69739=CARTESIAN_POINT ( 'NONE',  ( -42.52287095715005449, -23.72747288104469732, -1.053458166803227902 ) ) ;
#69740=CARTESIAN_POINT ( 'NONE',  ( 16.28047541435887879, -12.87082401369967677, 11.49999999999999645 ) ) ;
#69742=VECTOR ( 'NONE', #96730, 1000.000000000000114 ) ;
#69743=CARTESIAN_POINT ( 'NONE',  ( -106.6235367472416868, -24.65952944569304250, 1.056160979905701902 ) ) ;
#69744=CARTESIAN_POINT ( 'NONE',  ( 22.47986593085892437, -3.190245585651162230, 11.49999999999999645 ) ) ;
#69746=CARTESIAN_POINT ( 'NONE',  ( -69.60238025275721441, -23.73766607897669445, -1.055555164236460008 ) ) ;
#69747=CARTESIAN_POINT ( 'NONE',  ( -69.69245707645603716, -25.15756568742650856, 6.894249041125955380 ) ) ;
#69748=ORIENTED_EDGE ( 'NONE', *, *, #10027, .T. ) ;
#69749=CARTESIAN_POINT ( 'NONE',  ( -4.116507902937485142, 19.75820112358731251, 11.49999999999998934 ) ) ;
#69750=CARTESIAN_POINT ( 'NONE',  ( -108.6228709571500559, -23.95044443724992078, 10.65354141964649592 ) ) ;
#69751=CARTESIAN_POINT ( 'NONE',  ( -84.62287095715005592, -29.50250786944525672, 11.44777988621623521 ) ) ;
#69753=ORIENTED_EDGE ( 'NONE', *, *, #31967, .F. ) ;
#69755=CARTESIAN_POINT ( 'NONE',  ( 6.305670413343573699, 22.00876638805999974, -1.500000000000002220 ) ) ;
#69756=CARTESIAN_POINT ( 'NONE',  ( -79.34687923781920915, -25.26778825442007559, 5.960409282772108241 ) ) ;
#69757=AXIS2_PLACEMENT_3D ( 'NONE', #32114, #63087, #34006 ) ;
#69758=CARTESIAN_POINT ( 'NONE',  ( 2.319523670979641849, -21.48760272935114557, -1.500000000000002220 ) ) ;
#69760=CARTESIAN_POINT ( 'NONE',  ( 19.40856703110355852, -7.758221025823637262, 11.49999999999999645 ) ) ;
#69761=ORIENTED_EDGE ( 'NONE', *, *, #20727, .F. ) ;
#69762=AXIS2_PLACEMENT_3D ( 'NONE', #84475, #85974, #45434 ) ;
#69763=CARTESIAN_POINT ( 'NONE',  ( -124.5553389390244945, -24.15543982623907482, -0.2315651400026562945 ) ) ;
#69764=CARTESIAN_POINT ( 'NONE',  ( -14.32918165687622825, -16.72005635474405949, 11.49999999999998934 ) ) ;
#69765=EDGE_CURVE ( 'NONE', #11670, #90247, #25143, .T. ) ;
#69766=B_SPLINE_CURVE_WITH_KNOTS ( 'NONE', 3,
 ( #46201, #56839, #95377, #57341, #71552, #9641 ),
 .UNSPECIFIED., .F., .F.,
 ( 4, 2, 4 ),
 ( 1.570755371634072366E-05, 0.001396183895866090355, 0.002776660238015839915 ),
 .UNSPECIFIED. ) ;
#69768=CARTESIAN_POINT ( 'NONE',  ( -124.4728709571500360, -25.40674640480650126, 5.000950440061919799 ) ) ;
#69770=ORIENTED_EDGE ( 'NONE', *, *, #51535, .T. ) ;
#69772=EDGE_CURVE ( 'NONE', #21913, #30992, #44577, .T. ) ;
#69774=ORIENTED_EDGE ( 'NONE', *, *, #1793, .T. ) ;
#69775=DIRECTION ( 'NONE',  ( -3.773278334444166432E-23, 1.000000000000000000, 0.000000000000000000 ) ) ;
#69776=EDGE_LOOP ( 'NONE', ( #44242, #32446, #73569, #38104 ) ) ;
#69777=ORIENTED_EDGE ( 'NONE', *, *, #59491, .T. ) ;
#69779=CARTESIAN_POINT ( 'NONE',  ( -68.52287095715006160, -23.48783264082476308, -1.443836473390092356 ) ) ;
#69781=CARTESIAN_POINT ( 'NONE',  ( -12.04554601739387998, 16.56303510970703385, -1.500000000000002220 ) ) ;
#69783=DIRECTION ( 'NONE',  ( 0.000000000000000000, 0.9999999999976377785, 2.173523156925979975E-06 ) ) ;
#69784=CARTESIAN_POINT ( 'NONE',  ( -44.52203594336852888, -23.48783264082476663, -1.443836473390095021 ) ) ;
#69786=CARTESIAN_POINT ( 'NONE',  ( 1.165341552704713513, 22.26021350444069213, -1.500000000000002220 ) ) ;
#69791=CARTESIAN_POINT ( 'NONE',  ( -28.66728577581702808, -25.26248019189677763, 7.986659555697134039 ) ) ;
#69792=CARTESIAN_POINT ( 'NONE',  ( -1.025521031027718299, 20.81036885881322362, -1.500000000000002220 ) ) ;
#69794=CARTESIAN_POINT ( 'NONE',  ( -56.62287095715005592, -29.50248528299804818, 1.056150453629034924 ) ) ;
#69796=CARTESIAN_POINT ( 'NONE',  ( -31.62287095715005236, -24.65952944569304250, 1.056160979905689690 ) ) ;
#69797=CARTESIAN_POINT ( 'NONE',  ( 14.09988904737591575, 15.55221489148801872, -1.500000000000002220 ) ) ;
#69800=FACE_OUTER_BOUND ( 'NONE', #63068, .T. ) ;
#69804=DIRECTION ( 'NONE',  ( -1.000000000000000000, -3.773278334444166432E-23, -8.201307841325785021E-29 ) ) ;
#69805=CARTESIAN_POINT ( 'NONE',  ( -2.516727866726558460, 22.04588476715296963, 11.49999999999999645 ) ) ;
#69807=DIRECTION ( 'NONE',  ( 0.000000000000000000, -2.173523156925979552E-06, 0.9999999999976378895 ) ) ;
#69808=CARTESIAN_POINT ( 'NONE',  ( -44.62287095715004170, -23.96177878511307568, 10.65340807706330573 ) ) ;
#69810=CARTESIAN_POINT ( 'NONE',  ( 13.37577147909557773, 18.27418014603220442, -1.500000000000002220 ) ) ;
#69811=CARTESIAN_POINT ( 'NONE',  ( -93.52287095715009002, -23.48783264082477018, -1.443836473390088360 ) ) ;
#69812=ORIENTED_EDGE ( 'NONE', *, *, #2703, .F. ) ;
#69813=ORIENTED_EDGE ( 'NONE', *, *, #73179, .F. ) ;
#69816=CARTESIAN_POINT ( 'NONE',  ( -9.210493908506615313, -17.87979239004878451, -1.500000000000002220 ) ) ;
#69817=CARTESIAN_POINT ( 'NONE',  ( -34.62287095715005592, -29.50250243563736774, 8.947779886222150481 ) ) ;
#69820=B_SPLINE_CURVE_WITH_KNOTS ( 'NONE', 3,
 ( #4087, #49776, #19296, #35039, #49278, #65511 ),
 .UNSPECIFIED., .F., .F.,
 ( 4, 2, 4 ),
 ( 0.000000000000000000, 0.001380901958385393315, 0.002761803916770786630 ),
 .UNSPECIFIED. ) ;
#69822=CARTESIAN_POINT ( 'NONE',  ( 3.003370282714790562, 22.13870467353671856, -1.500000000000002220 ) ) ;
#69826=CARTESIAN_POINT ( 'NONE',  ( -89.62287095715004170, -24.64965695001468404, 8.947790433994180503 ) ) ;
#69827=ADVANCED_FACE ( 'NONE', ( #39059 ), #81450, .T. ) ;
#69829=CARTESIAN_POINT ( 'NONE',  ( -116.5228709571499763, -23.95044443724992789, 10.65354141964649237 ) ) ;
#69830=EDGE_CURVE ( 'NONE', #99331, #27910, #48174, .T. ) ;
#69833=CARTESIAN_POINT ( 'NONE',  ( 3.994393897313025743, -19.14333888664780048, -1.500000000000002220 ) ) ;
#69837=CARTESIAN_POINT ( 'NONE',  ( 4.199879391047538491, -21.09745483596041282, -1.500000000000002220 ) ) ;
#69838=CARTESIAN_POINT ( 'NONE',  ( -62.52287095715011844, -23.96177878511310055, 10.65340807706330217 ) ) ;
#69839=EDGE_CURVE ( 'NONE', #56219, #61101, #5377, .T. ) ;
#69842=CARTESIAN_POINT ( 'NONE',  ( -107.5895376238167529, -23.47596703998600631, 11.44779298504227683 ) ) ;
#69843=CARTESIAN_POINT ( 'NONE',  ( 22.85402955525884394, -0.1436109537974766814, -1.500000000000002220 ) ) ;
#69846=CARTESIAN_POINT ( 'NONE',  ( -42.52287095715004739, -23.48783264083366973, -1.443836473376261642 ) ) ;
#69847=CARTESIAN_POINT ( 'NONE',  ( 7.329891291799937925, -18.66831812819665970, 11.49999999999999645 ) ) ;
#69848=DIRECTION ( 'NONE',  ( 0.000000000000000000, -2.173523156925979552E-06, 0.9999999999976378895 ) ) ;
#69849=CARTESIAN_POINT ( 'NONE',  ( -100.6228709571500559, -29.50248789122583659, 2.256150453626215580 ) ) ;
#69853=EDGE_CURVE ( 'NONE', #69195, #57364, #66344, .T. ) ;
#69855=CARTESIAN_POINT ( 'NONE',  ( -109.0206074541901415, -25.23913850168018769, 3.730511194984860612 ) ) ;
#69856=CARTESIAN_POINT ( 'NONE',  ( -12.31242093702619123, -17.95196869449987531, -1.500000000000002220 ) ) ;
#69857=CARTESIAN_POINT ( 'NONE',  ( -68.93918693012690824, -29.50249643036528369, 6.184859213151739254 ) ) ;
#69858=CARTESIAN_POINT ( 'NONE',  ( 13.10555085358618221, -14.64361678476065087, -1.500000000000002220 ) ) ;
#69859=CARTESIAN_POINT ( 'NONE',  ( -122.6228709571500559, -24.51283580621365132, 0.6167428607019886933 ) ) ;
#69860=CARTESIAN_POINT ( 'NONE',  ( -109.7735670026218173, -25.27925862195693796, 5.109898703217436555 ) ) ;
#69861=CARTESIAN_POINT ( 'NONE',  ( -91.59442375792446001, -23.96169478059713498, 10.65365249895717881 ) ) ;
#69863=CARTESIAN_POINT ( 'NONE',  ( -1.637206367458305500, 20.51943892441452633, 11.49999999999999645 ) ) ;
#69865=CARTESIAN_POINT ( 'NONE',  ( -120.6245372636320639, -24.73486907724918638, 1.287355809206965684 ) ) ;
#69867=CARTESIAN_POINT ( 'NONE',  ( -46.62287095715004881, -24.65952944569304250, 1.056160979905693020 ) ) ;
#69868=FACE_OUTER_BOUND ( 'NONE', #70731, .T. ) ;
#69869=CARTESIAN_POINT ( 'NONE',  ( -74.52287095715009002, -23.72773821059536914, 11.05748984161097148 ) ) ;
#69871=CARTESIAN_POINT ( 'NONE',  ( -25.88669879221086134, -24.61459842209443494, 7.002165747688067654 ) ) ;
#69873=EDGE_CURVE ( 'NONE', #23809, #84257, #81006, .T. ) ;
#69874=CARTESIAN_POINT ( 'NONE',  ( 13.09964176094197441, 18.96253433080681106, 11.49999999999999645 ) ) ;
#69875=CARTESIAN_POINT ( 'NONE',  ( 10.87194125936840194, 20.03610521102953257, 11.49999999999998934 ) ) ;
#69876=CARTESIAN_POINT ( 'NONE',  ( -74.50754834148092698, -24.15543982623906771, -0.2315651400026650653 ) ) ;
#69877=CARTESIAN_POINT ( 'NONE',  ( -88.52287095715003318, -24.51283580621364777, 0.6167428607019784792 ) ) ;
#69878=CARTESIAN_POINT ( 'NONE',  ( -123.5228709571500474, -24.34917612406837151, 0.1852690917426585981 ) ) ;
#69879=CARTESIAN_POINT ( 'NONE',  ( -22.41777205227948855, 0.6913007675000180097, 11.49999999999999645 ) ) ;
#69880=ORIENTED_EDGE ( 'NONE', *, *, #98794, .F. ) ;
#69882=CARTESIAN_POINT ( 'NONE',  ( -43.52287095715006160, -24.64965694238406613, 8.947790433994205372 ) ) ;
#69883=CARTESIAN_POINT ( 'NONE',  ( 15.37660858059359725, 15.65766701038582021, 11.49999999999998934 ) ) ;
#69884=ADVANCED_FACE ( 'NONE', ( #4391 ), #98714, .F. ) ;
#69889=LINE ( 'NONE', #880, #1489 ) ;
#69891=CARTESIAN_POINT ( 'NONE',  ( -13.28352777634190396, 15.58691228024164310, 11.49999999999998934 ) ) ;
#69893=EDGE_LOOP ( 'NONE', ( #29829, #48699, #30576, #60357 ) ) ;
#69894=ORIENTED_EDGE ( 'NONE', *, *, #77885, .T. ) ;
#69895=ORIENTED_EDGE ( 'NONE', *, *, #12024, .F. ) ;
#69896=CARTESIAN_POINT ( 'NONE',  ( -20.32320236877023589, 10.94715076914730290, 11.49999999999998934 ) ) ;
#69897=CARTESIAN_POINT ( 'NONE',  ( -82.52287095715003318, -24.50216790748205042, 0.6166512839542531710 ) ) ;
#69898=CARTESIAN_POINT ( 'NONE',  ( 13.48481281434462531, 15.16087405922196041, -1.500000000000002220 ) ) ;
#69899=ORIENTED_EDGE ( 'NONE', *, *, #7325, .F. ) ;
#69901=CARTESIAN_POINT ( 'NONE',  ( -92.60130187865181028, -23.48783264082478084, -1.443836473390064157 ) ) ;
#69903=CARTESIAN_POINT ( 'NONE',  ( -127.6228709571500559, -29.50250243563736774, 8.947779886222132717 ) ) ;
#69904=CARTESIAN_POINT ( 'NONE',  ( -70.63225065262203373, -24.63355581998385091, 0.9682620441943861067 ) ) ;
#69905=CARTESIAN_POINT ( 'NONE',  ( 12.90647603486358364, 17.18646895862681134, 11.49999999999999645 ) ) ;
#69907=PLANE ( 'NONE',  #72743 ) ;
#69908=CARTESIAN_POINT ( 'NONE',  ( -61.56642141492948639, -23.48786465467240703, 11.44779295918255002 ) ) ;
#69909=( GEOMETRIC_REPRESENTATION_CONTEXT ( 3 ) GLOBAL_UNCERTAINTY_ASSIGNED_CONTEXT ( ( #54023 ) ) GLOBAL_UNIT_ASSIGNED_CONTEXT ( ( #16563, #66149, #25687 ) ) REPRESENTATION_CONTEXT ( 'NONE', 'WORKASPACE' ) );
#69911=CARTESIAN_POINT ( 'NONE',  ( 12.20387445076365296, 16.77033177596414504, 11.49999999999998934 ) ) ;
#69914=CARTESIAN_POINT ( 'NONE',  ( -70.75516858542015086, -25.30843098343074971, 4.197529876663087300 ) ) ;
#69916=CARTESIAN_POINT ( 'NONE',  ( -111.5187044900002746, -23.96169478059714564, 10.65365249895717348 ) ) ;
#69921=CARTESIAN_POINT ( 'NONE',  ( -65.58911965655261156, -24.52300882791528380, 0.6510814631126250474 ) ) ;
#69922=CARTESIAN_POINT ( 'NONE',  ( -21.70078857174656761, -3.768841730229552045, 11.49999999999999645 ) ) ;
#69923=CARTESIAN_POINT ( 'NONE',  ( -89.50575723802535322, -24.51419770103157703, 9.386484678747176957 ) ) ;
#69924=CARTESIAN_POINT ( 'NONE',  ( 22.42242567092132433, 2.420433022335332751, 11.49999999999998934 ) ) ;
#69925=CARTESIAN_POINT ( 'NONE',  ( 6.892386425805808514, -19.84609432511738447, -1.500000000000002220 ) ) ;
#69927=ORIENTED_EDGE ( 'NONE', *, *, #23422, .T. ) ;
#69929=CARTESIAN_POINT ( 'NONE',  ( -59.62287095715004881, -24.64965695001468404, 8.947790433994185832 ) ) ;
#69932=ORIENTED_EDGE ( 'NONE', *, *, #21166, .F. ) ;
#69933=CARTESIAN_POINT ( 'NONE',  ( 19.82261944725993175, 7.364942908566579405, 11.49999999999998934 ) ) ;
#69934=CARTESIAN_POINT ( 'NONE',  ( -67.58953762381671027, -23.47593901973091235, -1.443836447539006196 ) ) ;
#69935=CARTESIAN_POINT ( 'NONE',  ( -51.71530383401179876, -25.26040974995711608, 6.909342197498395066 ) ) ;
#69936=CARTESIAN_POINT ( 'NONE',  ( -49.56659911537192897, -25.28200315853347035, 4.244126846616177673 ) ) ;
#69937=CARTESIAN_POINT ( 'NONE',  ( -79.55620429048339304, -24.64898659630528854, 1.056161002820828143 ) ) ;
#69938=DIRECTION ( 'NONE',  ( -3.773278334453079030E-23, 0.9999999999976377785, 2.173523156925979128E-06 ) ) ;
#69939=CARTESIAN_POINT ( 'NONE',  ( 21.88104185797606505, 3.448541436957560880, -1.500000000000002220 ) ) ;
#69940=CARTESIAN_POINT ( 'NONE',  ( -71.64476510811557830, -23.73766607897669800, -1.055555164236456012 ) ) ;
#69941=EDGE_CURVE ( 'NONE', #2526, #88549, #20290, .T. ) ;
#69942=B_SPLINE_CURVE_WITH_KNOTS ( 'NONE', 3,
 ( #38894, #95056, #64642, #334, #87442, #86938, #79324, #49403, #48896, #9818, #46513, #77442, #61755, #69855, #87951, #34167, #62249, #72228 ),
 .UNSPECIFIED., .F., .F.,
 ( 4, 2, 2, 2, 2, 2, 2, 2, 4 ),
 ( 1.411962612463446054E-17, 0.0002633899507887005873, 0.0005267799015773870800, 0.0007901698523660736270, 0.001053559803154760065, 0.001316949753943446504, 0.001580339704732133159, 0.001843729655520819598, 0.002107119606309506253 ),
 .UNSPECIFIED. ) ;
#69944=CARTESIAN_POINT ( 'NONE',  ( -51.81420417462592809, -25.24860145185455806, 5.643201866869797634 ) ) ;
#69946=CARTESIAN_POINT ( 'NONE',  ( -43.62287095715006302, -23.96127896941632685, -0.6493128931037891460 ) ) ;
#69947=CARTESIAN_POINT ( 'NONE',  ( -41.86208256938783023, -25.26663232696201433, 4.025867116275735569 ) ) ;
#69948=CARTESIAN_POINT ( 'NONE',  ( -39.62287095715005592, -24.64965695001468404, 8.947790433994187609 ) ) ;
#69949=CARTESIAN_POINT ( 'NONE',  ( 9.746180923669104601, -16.83516941858706417, 11.49999999999998934 ) ) ;
#69950=ADVANCED_FACE ( 'NONE', ( #36331 ), #3896, .T. ) ;
#69951=CARTESIAN_POINT ( 'NONE',  ( -9.924231251898440576, -18.97836718215353713, 11.49999999999998934 ) ) ;
#69952=CARTESIAN_POINT ( 'NONE',  ( -38.52287095715006870, -24.66019654487199730, 8.947790411086121054 ) ) ;
#69953=CARTESIAN_POINT ( 'NONE',  ( -60.54140983439796742, -24.52399227489757649, 9.353111116819363247 ) ) ;
#69954=B_SPLINE_CURVE_WITH_KNOTS ( 'NONE', 3,
 ( #73501, #94331, #3993, #52655 ),
 .UNSPECIFIED., .F., .F.,
 ( 4, 4 ),
 ( 0.6702645439819958639, 0.6792709752541115087 ),
 .UNSPECIFIED. ) ;
#69956=EDGE_CURVE ( 'NONE', #19418, #81354, #45828, .T. ) ;
#69957=CARTESIAN_POINT ( 'NONE',  ( -51.62816867347140715, -24.51314013834315730, 0.6176544820404110681 ) ) ;
#69958=CARTESIAN_POINT ( 'NONE',  ( -101.2905359165590227, -25.18440123917106277, 3.812648632975031315 ) ) ;
#69959=CARTESIAN_POINT ( 'NONE',  ( 13.97002500213282516, -17.90638934399130733, -1.500000000000002220 ) ) ;
#69960=CARTESIAN_POINT ( 'NONE',  ( -98.51906589821315663, -23.73766607897669800, -1.055555164236454013 ) ) ;
#69961=CARTESIAN_POINT ( 'NONE',  ( -62.62287095715002039, -24.35013146730203815, 9.818937971375111928 ) ) ;
#69962=CARTESIAN_POINT ( 'NONE',  ( -4.880483578727112359, 19.22116399702514045, 11.49999999999999645 ) ) ;
#69963=CARTESIAN_POINT ( 'NONE',  ( -123.6266590520278186, -23.48786465467241769, 11.44779295918253759 ) ) ;
#69966=EDGE_CURVE ( 'NONE', #34234, #53182, #14362, .T. ) ;
#69967=FACE_OUTER_BOUND ( 'NONE', #93607, .T. ) ;
#69968=CARTESIAN_POINT ( 'NONE',  ( -66.52287095715006160, -29.50250243563736774, 8.947779886222143375 ) ) ;
#69969=FACE_OUTER_BOUND ( 'NONE', #23745, .T. ) ;
#69970=CARTESIAN_POINT ( 'NONE',  ( 20.17453868081960167, 7.849935799312063089, 11.49999999999998934 ) ) ;
#69971=CARTESIAN_POINT ( 'NONE',  ( -67.52287095715006160, -29.50250243563736774, 8.947779886222143375 ) ) ;
#69972=CARTESIAN_POINT ( 'NONE',  ( -5.977879402576776968, -18.46583800616800630, -1.500000000000002220 ) ) ;
#69973=CARTESIAN_POINT ( 'NONE',  ( -61.62287095715004170, -23.72773821059536559, 11.05748984161097503 ) ) ;
#69974=CARTESIAN_POINT ( 'NONE',  ( -18.24533751216517885, 7.751685665592884078, 11.49999999999998934 ) ) ;
#69978=CARTESIAN_POINT ( 'NONE',  ( 12.54693703879240196, 16.07252283493236433, 11.49999999999999645 ) ) ;
#69979=DIRECTION ( 'NONE',  ( 1.000000000000000000, 3.773278334444167608E-23, 8.201307833595939069E-29 ) ) ;
#69980=CARTESIAN_POINT ( 'NONE',  ( -104.5228709571501184, -23.48783264082477373, -1.443836473390087027 ) ) ;
#69982=CARTESIAN_POINT ( 'NONE',  ( -80.40673297319085577, -25.03305104182449270, 7.562216455819397609 ) ) ;
#69984=CARTESIAN_POINT ( 'NONE',  ( -49.35191700208513765, -25.25214480681022522, 5.185240423550362188 ) ) ;
#69985=CARTESIAN_POINT ( 'NONE',  ( -128.6228709571500417, -23.96127896941633750, -0.6493128931037734919 ) ) ;
#69986=FACE_OUTER_BOUND ( 'NONE', #40583, .T. ) ;
#69987=CARTESIAN_POINT ( 'NONE',  ( 4.282148337517553749, -19.64591042314588165, 11.49999999999998934 ) ) ;
#69993=CARTESIAN_POINT ( 'NONE',  ( -9.675568039816649701, -20.77828039667204862, 11.49999999999999645 ) ) ;
#69994=CARTESIAN_POINT ( 'NONE',  ( 13.97002500213282516, -17.90638934399130733, 11.49999999999998934 ) ) ;
#69995=ORIENTED_EDGE ( 'NONE', *, *, #26630, .T. ) ;
#69998=CARTESIAN_POINT ( 'NONE',  ( -38.53313680577858236, -24.51419770103157347, 9.386484678747176957 ) ) ;
#69999=DIRECTION ( 'NONE',  ( 0.000000000000000000, 2.173523156925980399E-06, -0.9999999999976378895 ) ) ;
#70000=CARTESIAN_POINT ( 'NONE',  ( -128.5899664246173302, -23.96169478059714919, 10.65365249895716993 ) ) ;
#70003=B_SPLINE_CURVE_WITH_KNOTS ( 'NONE', 3,
 ( #82093, #66393, #56780, #43042 ),
 .UNSPECIFIED., .F., .F.,
 ( 4, 4 ),
 ( 0.000000000000000000, 9.999999999998898659E-05 ),
 .UNSPECIFIED. ) ;
#70005=ORIENTED_EDGE ( 'NONE', *, *, #71638, .T. ) ;
#70006=CARTESIAN_POINT ( 'NONE',  ( -16.54958403137900191, 11.88860064210666856, -1.500000000000002220 ) ) ;
#70007=B_SPLINE_CURVE_WITH_KNOTS ( 'NONE', 3,
 ( #68146, #22439, #20455, #84352, #14835, #75247 ),
 .UNSPECIFIED., .F., .F.,
 ( 4, 2, 4 ),
 ( 0.000000000000000000, 0.001380764517854766050, 0.002761529035709532100 ),
 .UNSPECIFIED. ) ;
#70009=CARTESIAN_POINT ( 'NONE',  ( -19.49525799874905729, 12.17417675796824561, 11.49999999999998934 ) ) ;
#70010=CARTESIAN_POINT ( 'NONE',  ( -54.62367911701477396, -24.66019654487199375, 8.947790411086119278 ) ) ;
#70011=VERTEX_POINT ( 'NONE', #21090 ) ;
#70012=CARTESIAN_POINT ( 'NONE',  ( -108.5505251014125321, -24.51419770103157347, 9.386484678747168076 ) ) ;
#70014=CARTESIAN_POINT ( 'NONE',  ( -111.5228709571500332, -23.95044443724993144, 10.65354141964649237 ) ) ;
#70015=CARTESIAN_POINT ( 'NONE',  ( 8.224165413489119558, 19.69228431130148493, 11.49999999999999645 ) ) ;
#70018=EDGE_LOOP ( 'NONE', ( #29634, #48576, #80280, #82966 ) ) ;
#70019=CARTESIAN_POINT ( 'NONE',  ( 21.63176498729014341, 4.993826359924048219, 11.49999999999998934 ) ) ;
#70020=AXIS2_PLACEMENT_3D ( 'NONE', #66139, #27054, #11327 ) ;
#70021=CARTESIAN_POINT ( 'NONE',  ( 7.614520588612671226, -19.20288753073135268, -1.500000000000002220 ) ) ;
#70022=EDGE_CURVE ( 'NONE', #49913, #98343, #4683, .T. ) ;
#70025=CARTESIAN_POINT ( 'NONE',  ( -112.6228709571500701, -23.95044443724992433, 10.65354141964649948 ) ) ;
#70026=CARTESIAN_POINT ( 'NONE',  ( -95.51719868888432075, -23.85049219812686161, 10.88485053497527133 ) ) ;
#70027=VERTEX_POINT ( 'NONE', #52056 ) ;
#70028=CARTESIAN_POINT ( 'NONE',  ( -91.59781571226605479, -23.73766607897670156, -1.055555164236454235 ) ) ;
#70029=ADVANCED_FACE ( 'NONE', ( #57680 ), #99692, .F. ) ;
#70030=B_SPLINE_CURVE_WITH_KNOTS ( 'NONE', 3,
 ( #77477, #31824, #78982, #62793, #54668, #55175, #93708, #24694 ),
 .UNSPECIFIED., .F., .F.,
 ( 4, 2, 2, 4 ),
 ( -0.001224554619866349532, -0.0002241820295893679187, 0.0007761905606876136950, 0.002776935741241577139 ),
 .UNSPECIFIED. ) ;
#70032=CARTESIAN_POINT ( 'NONE',  ( -58.63776154008928643, -24.15620529776628089, 10.23563542870660470 ) ) ;
#70033=PLANE ( 'NONE',  #90838 ) ;
#70034=CARTESIAN_POINT ( 'NONE',  ( -5.744250498300313090, 20.02623800365557472, -1.500000000000002220 ) ) ;
#70035=CARTESIAN_POINT ( 'NONE',  ( 8.107222467604051630, 20.28165043084963060, 11.49999999999999645 ) ) ;
#70036=CARTESIAN_POINT ( 'NONE',  ( -91.23534077628075067, -25.22391154813774605, 6.409327647370976599 ) ) ;
#70037=CARTESIAN_POINT ( 'NONE',  ( -78.55031912633015168, -24.15620529776628445, 10.23563542870660292 ) ) ;
#70038=CARTESIAN_POINT ( 'NONE',  ( -22.07377061809603092, 4.253497373390751513, -1.500000000000002220 ) ) ;
#70039=ADVANCED_FACE ( 'NONE', ( #68775 ), #83991, .T. ) ;
#70041=CARTESIAN_POINT ( 'NONE',  ( -85.62287095715005592, -29.50250786944525672, 11.44777988621623344 ) ) ;
#70046=EDGE_CURVE ( 'NONE', #74266, #32974, #85482, .T. ) ;
#70047=ORIENTED_EDGE ( 'NONE', *, *, #31209, .F. ) ;
#70048=EDGE_LOOP ( 'NONE', ( #89155, #76738, #51489, #29081 ) ) ;
#70049=ORIENTED_EDGE ( 'NONE', *, *, #23760, .T. ) ;
#70050=CARTESIAN_POINT ( 'NONE',  ( -5.188002292566340934, -20.72503599944539587, -1.500000000000002220 ) ) ;
#70051=ORIENTED_EDGE ( 'NONE', *, *, #28443, .T. ) ;
#70052=CARTESIAN_POINT ( 'NONE',  ( -13.06023916655064276, -16.53025015627232719, -1.500000000000002220 ) ) ;
#70053=CARTESIAN_POINT ( 'NONE',  ( -30.55377735246407411, -24.38452336476660065, 0.3015907515355735202 ) ) ;
#70054=CARTESIAN_POINT ( 'NONE',  ( 15.91301918423788919, -12.03417825965012433, -1.500000000000002220 ) ) ;
#70055=CARTESIAN_POINT ( 'NONE',  ( -114.5228709571500616, -23.48786465467241769, 11.44779295918253936 ) ) ;
#70057=CARTESIAN_POINT ( 'NONE',  ( 10.07166557822571207, 19.55152498600455857, -1.500000000000002220 ) ) ;
#70060=CARTESIAN_POINT ( 'NONE',  ( -74.58953762381672448, -24.64965694238407679, 8.947790433994656567 ) ) ;
#70063=CARTESIAN_POINT ( 'NONE',  ( -9.832896139050584239, -18.40278743011522877, 11.49999999999999645 ) ) ;
#70065=DIRECTION ( 'NONE',  ( -3.773278334444166432E-23, 1.000000000000000000, 0.000000000000000000 ) ) ;
#70066=CARTESIAN_POINT ( 'NONE',  ( -20.48352523709943185, -22.69084714409266823, 11.44779298504228215 ) ) ;
#70067=CARTESIAN_POINT ( 'NONE',  ( 11.00477826368897283, 18.22718707545001138, -1.500000000000002220 ) ) ;
#70068=FACE_OUTER_BOUND ( 'NONE', #17096, .T. ) ;
#70069=CARTESIAN_POINT ( 'NONE',  ( -107.5116926678866207, -24.66019654487199730, 8.947790411086115725 ) ) ;
#70070=ADVANCED_FACE ( 'NONE', ( #75873 ), #4496, .T. ) ;
#70072=CARTESIAN_POINT ( 'NONE',  ( -70.65754726777662142, -25.12112739299269037, 7.112216829152949948 ) ) ;
#70073=CARTESIAN_POINT ( 'NONE',  ( 14.32739804834607256, 17.34395043298086847, -1.500000000000002220 ) ) ;
#70074=AXIS2_PLACEMENT_3D ( 'NONE', #98135, #28148, #21506 ) ;
#70075=B_SPLINE_SURFACE_WITH_KNOTS ( 'NONE', 3, 3, ( 
 ( #94754, #18626, #86145, #16627 ),
 ( #47599, #70935, #94253, #55718 ),
 ( #17130, #97258, #34866, #49604 ),
 ( #27750, #42988, #51092, #26750 ),
 ( #19627, #74422, #57714, #58700 ),
 ( #59206, #50099, #11517, #50589 ),
 ( #4915, #89153, #73926, #90148 ) ),
 .UNSPECIFIED., .F., .F., .F.,
 ( 4, 3, 4 ),
 ( 4, 4 ),
 ( 0.7945040050992245861, 0.8970133687736507877, 0.9995227324480768782 ),
 ( 0.8697150038779488668, 0.8711292465922757522 ),
 .UNSPECIFIED. ) ;
#70077=CARTESIAN_POINT ( 'NONE',  ( -129.5562042904833788, -24.66019654487200441, 8.947790411086121054 ) ) ;
#70081=CARTESIAN_POINT ( 'NONE',  ( -8.027368788987615744, 17.96763083595211441, 11.49999999999999645 ) ) ;
#70082=DIRECTION ( 'NONE',  ( 0.000000000000000000, -2.173523156925980399E-06, 0.9999999999976378895 ) ) ;
#70083=DIRECTION ( 'NONE',  ( 3.773278334444167608E-23, -1.000000000000000000, 0.000000000000000000 ) ) ;
#70084=ORIENTED_EDGE ( 'NONE', *, *, #8558, .T. ) ;
#70085=EDGE_CURVE ( 'NONE', #69320, #71901, #77858, .T. ) ;
#70086=CARTESIAN_POINT ( 'NONE',  ( -89.52287095715001897, -23.95044443724991723, 10.65354141964648882 ) ) ;
#70087=CARTESIAN_POINT ( 'NONE',  ( -115.5228709571500616, -29.50248789122583659, 2.256150453626215580 ) ) ;
#70088=CARTESIAN_POINT ( 'NONE',  ( -100.2069791292054504, -25.31439543413117477, 5.245324408949481487 ) ) ;
#70089=B_SPLINE_CURVE_WITH_KNOTS ( 'NONE', 3,
 ( #67031, #73627, #43185, #88861 ),
 .UNSPECIFIED., .F., .F.,
 ( 4, 4 ),
 ( 0.000000000000000000, 9.999999999998897304E-05 ),
 .UNSPECIFIED. ) ;
#70090=EDGE_CURVE ( 'NONE', #95766, #15382, #36124, .T. ) ;
#70091=DIRECTION ( 'NONE',  ( -3.773278334444166432E-23, 1.000000000000000000, 0.000000000000000000 ) ) ;
#70092=CARTESIAN_POINT ( 'NONE',  ( 18.24634267693259559, -7.554628487255452107, 11.49999999999998934 ) ) ;
#70093=ADVANCED_FACE ( 'NONE', ( #6374 ), #55051, .T. ) ;
#70095=B_SPLINE_CURVE_WITH_KNOTS ( 'NONE', 3,
 ( #14576, #75967, #85088, #46538, #84589, #37428 ),
 .UNSPECIFIED., .F., .F.,
 ( 4, 2, 4 ),
 ( 1.570887131794333942E-05, 0.001396322306279759555, 0.002776935741241575838 ),
 .UNSPECIFIED. ) ;
#70096=AXIS2_PLACEMENT_3D ( 'NONE', #19049, #3355, #18551 ) ;
#70097=CARTESIAN_POINT ( 'NONE',  ( -110.2723855490748122, -25.19526345475334850, 3.295595324081435074 ) ) ;
#70099=ORIENTED_EDGE ( 'NONE', *, *, #23050, .F. ) ;
#70103=DIRECTION ( 'NONE',  ( -3.773278334453080206E-23, 0.9999999999976377785, 2.173523156925979975E-06 ) ) ;
#70105=CARTESIAN_POINT ( 'NONE',  ( -123.6228709571500559, -23.47593901973091235, -1.443836447538997536 ) ) ;
#70106=CARTESIAN_POINT ( 'NONE',  ( -107.5875604241846730, -24.51314013834315730, 0.6176544820404215042 ) ) ;
#70107=CARTESIAN_POINT ( 'NONE',  ( -16.75416981316412190, 10.96944243606782443, -1.500000000000002220 ) ) ;
#70108=CARTESIAN_POINT ( 'NONE',  ( -99.49608100277511369, -25.10935113139711206, 3.179641471686016629 ) ) ;
#70109=CARTESIAN_POINT ( 'NONE',  ( -45.62377148096768309, -25.00182538069146787, 7.747789668545045139 ) ) ;
#70110=VERTEX_POINT ( 'NONE', #9359 ) ;
#70111=AXIS2_PLACEMENT_3D ( 'NONE', #68713, #38243, #29140 ) ;
#70113=PLANE ( 'NONE',  #16160 ) ;
#70114=CARTESIAN_POINT ( 'NONE',  ( -110.0449441895338509, -25.29012733315208195, 3.330200468167525685 ) ) ;
#70115=CARTESIAN_POINT ( 'NONE',  ( -74.62287095715005592, -23.48786465467241058, 11.44779295918254469 ) ) ;
#70116=DIRECTION ( 'NONE',  ( 0.000000000000000000, 0.9999999999976377785, 2.173523156925979128E-06 ) ) ;
#70121=CARTESIAN_POINT ( 'NONE',  ( -40.52287095715006870, -24.51254535375849031, 9.355368624242066389 ) ) ;
#70123=CARTESIAN_POINT ( 'NONE',  ( -2.359408512905806443, -20.17289352931189583, 11.49999999999998934 ) ) ;
#70125=FACE_OUTER_BOUND ( 'NONE', #6217, .T. ) ;
#70127=ORIENTED_EDGE ( 'NONE', *, *, #46621, .F. ) ;
#70128=PLANE ( 'NONE',  #6447 ) ;
#70129=CARTESIAN_POINT ( 'NONE',  ( -13.04681709000290013, -15.30929823114697541, -1.500000000000002220 ) ) ;
#70130=CARTESIAN_POINT ( 'NONE',  ( -16.61111445048470614, -13.04167290785011701, 11.49999999999999645 ) ) ;
#70131=CARTESIAN_POINT ( 'NONE',  ( -4.051365815588555463, -21.74199345402511696, 11.49999999999998934 ) ) ;
#70132=CARTESIAN_POINT ( 'NONE',  ( -6.092534927433182368, -19.63929903328317295, 11.49999999999998934 ) ) ;
#70134=EDGE_CURVE ( 'NONE', #39828, #26090, #35929, .T. ) ;
#70136=VERTEX_POINT ( 'NONE', #1761 ) ;
#70137=DIRECTION ( 'NONE',  ( 0.000000000000000000, 0.9999999999976377785, 2.173523156925979975E-06 ) ) ;
#70140=CARTESIAN_POINT ( 'NONE',  ( -109.5228709571500616, -24.33927499327855415, 9.819080762295811837 ) ) ;
#70141=ORIENTED_EDGE ( 'NONE', *, *, #78721, .F. ) ;
#70145=CARTESIAN_POINT ( 'NONE',  ( -49.21454750704995007, -25.12863070112381791, 7.069183623698430452 ) ) ;
#70146=CARTESIAN_POINT ( 'NONE',  ( -68.54922812267722065, -24.15620529776627734, 10.23563542870660825 ) ) ;
#70147=CARTESIAN_POINT ( 'NONE',  ( -3.285303218690974525, -20.39892020120133154, -1.500000000000002220 ) ) ;
#70148=CARTESIAN_POINT ( 'NONE',  ( 7.158504886898216846, -20.39052948596947346, 11.49999999999999645 ) ) ;
#70149=ORIENTED_EDGE ( 'NONE', *, *, #7158, .F. ) ;
#70151=ADVANCED_FACE ( 'NONE', ( #79370 ), #72279, .F. ) ;
#70154=CARTESIAN_POINT ( 'NONE',  ( -16.90645664988545249, 14.66980924573920397, -1.500000000000002220 ) ) ;
#70157=CARTESIAN_POINT ( 'NONE',  ( -47.62369827702862324, -24.66019654487199730, 8.947790411086117501 ) ) ;
#70160=CARTESIAN_POINT ( 'NONE',  ( -117.5798424949460923, -25.31863975941917388, 6.461805294873899541 ) ) ;
#70161=CARTESIAN_POINT ( 'NONE',  ( -120.6228709571500559, -25.00182538069145721, 7.747789668545100206 ) ) ;
#70163=CARTESIAN_POINT ( 'NONE',  ( 13.94627346685978075, -15.57361473980792255, 11.49999999999998934 ) ) ;
#70164=ORIENTED_EDGE ( 'NONE', *, *, #92769, .T. ) ;
#70166=EDGE_LOOP ( 'NONE', ( #6343, #64803, #62598, #62822 ) ) ;
#70167=FACE_OUTER_BOUND ( 'NONE', #25857, .T. ) ;
#70168=CARTESIAN_POINT ( 'NONE',  ( 16.91677535067316995, -12.78530099663392505, -1.500000000000002220 ) ) ;
#70169=ORIENTED_EDGE ( 'NONE', *, *, #88650, .F. ) ;
#70170=CARTESIAN_POINT ( 'NONE',  ( -79.52287095715006160, -24.64965694238575011, 8.947790433994198267 ) ) ;
#70171=CARTESIAN_POINT ( 'NONE',  ( 19.81658424304261246, 9.080307684375437560, 11.49999999999998934 ) ) ;
#70172=LINE ( 'NONE', #22476, #56265 ) ;
#70173=PLANE ( 'NONE',  #72897 ) ;
#70174=CARTESIAN_POINT ( 'NONE',  ( -35.52287095715006160, -24.91570333825474037, 8.075032458260901436 ) ) ;
#70175=CARTESIAN_POINT ( 'NONE',  ( 20.57308398666954119, -7.222494929537193187, -1.500000000000002220 ) ) ;
#70176=CARTESIAN_POINT ( 'NONE',  ( -30.57287095715005876, -25.25639193976267194, 6.126332763130458936 ) ) ;
#70180=ADVANCED_FACE ( 'NONE', ( #63169 ), #94094, .T. ) ;
#70181=ORIENTED_EDGE ( 'NONE', *, *, #3964, .F. ) ;
#70184=ADVANCED_FACE ( 'NONE', ( #10363 ), #64687, .T. ) ;
#70185=ORIENTED_EDGE ( 'NONE', *, *, #17580, .T. ) ;
#70187=CARTESIAN_POINT ( 'NONE',  ( -28.24811442358726410, -24.84257439951912616, 2.397443450879609639 ) ) ;
#70189=CARTESIAN_POINT ( 'NONE',  ( 4.903939382885006637, -20.63555827282145572, -1.500000000000002220 ) ) ;
#70190=CARTESIAN_POINT ( 'NONE',  ( -79.52287095715006160, -24.65952944569304961, 1.056160979905698794 ) ) ;
#70191=FACE_OUTER_BOUND ( 'NONE', #12749, .T. ) ;
#70192=EDGE_CURVE ( 'NONE', #1913, #4586, #90385, .T. ) ;
#70194=CARTESIAN_POINT ( 'NONE',  ( -128.5228709571500758, -23.47593901973090524, -1.443836447538996204 ) ) ;
#70196=CARTESIAN_POINT ( 'NONE',  ( 17.66168439605153395, -8.020940556088177686, 11.49999999999998934 ) ) ;
#70197=CARTESIAN_POINT ( 'NONE',  ( -41.89292675774235875, -25.11539320593059443, 2.804431443241629740 ) ) ;
#70199=CARTESIAN_POINT ( 'NONE',  ( -7.634514033349506512, -17.95459398628807435, 11.49999999999999645 ) ) ;
#70200=CARTESIAN_POINT ( 'NONE',  ( -34.58953762381671737, -23.48783264082478084, -1.443836473390074149 ) ) ;
#70202=B_SPLINE_CURVE_WITH_KNOTS ( 'NONE', 3,
 ( #65963, #26873, #42117, #80659 ),
 .UNSPECIFIED., .F., .F.,
 ( 4, 4 ),
 ( 0.000000000000000000, 9.999999999998897304E-05 ),
 .UNSPECIFIED. ) ;
#70204=ORIENTED_EDGE ( 'NONE', *, *, #37682, .T. ) ;
#70206=CARTESIAN_POINT ( 'NONE',  ( -103.6228709571500417, -23.47596703998600631, 11.44779298504227860 ) ) ;
#70208=DIRECTION ( 'NONE',  ( 1.000000000000000000, 3.773278334444167608E-23, 8.201307833595939069E-29 ) ) ;
#70209=EDGE_CURVE ( 'NONE', #96384, #125, #58947, .T. ) ;
#70210=CARTESIAN_POINT ( 'NONE',  ( -93.54679903806243146, -24.51419770103157703, 9.386484678747164523 ) ) ;
#70211=CARTESIAN_POINT ( 'NONE',  ( 19.59260286812380514, -1.442238090573773501, 11.49999999999998934 ) ) ;
#70212=B_SPLINE_SURFACE_WITH_KNOTS ( 'NONE', 3, 3, ( 
 ( #47468, #2804, #70807, #87020 ),
 ( #33741, #48476, #64722, #18506 ),
 ( #47969, #78894, #49480, #63715 ),
 ( #41353, #1296, #40844, #32229 ),
 ( #80410, #10395, #56087, #72307 ),
 ( #79403, #63203, #71811, #33232 ),
 ( #94126, #64212, #25624, #56596 ) ),
 .UNSPECIFIED., .F., .F., .F.,
 ( 4, 3, 4 ),
 ( 4, 4 ),
 ( 0.7945040050992243641, 0.8970133687736502326, 0.9995227324480761011 ),
 ( 0.4396057071469119393, 0.4408213828681695756 ),
 .UNSPECIFIED. ) ;
#70213=CARTESIAN_POINT ( 'NONE',  ( -41.46533095918948675, -25.31583583508971813, 4.218578428352230070 ) ) ;
#70215=CARTESIAN_POINT ( 'NONE',  ( -21.50746323947805649, 1.722430922125298247, 11.49999999999998934 ) ) ;
#70216=CARTESIAN_POINT ( 'NONE',  ( -40.48566607648301385, -24.52300882791530157, 0.6510814631126360386 ) ) ;
#70219=CARTESIAN_POINT ( 'NONE',  ( 21.63105218614105851, 7.968772182826888262, -1.500000000000002220 ) ) ;
#70221=CARTESIAN_POINT ( 'NONE',  ( -93.62801744632055545, -24.34968618360934300, 0.1864209137778838898 ) ) ;
#70222=CARTESIAN_POINT ( 'NONE',  ( -115.5895376238167245, -23.47593901973091235, -1.443836447538997536 ) ) ;
#70223=CARTESIAN_POINT ( 'NONE',  ( -121.6267055903540637, -23.73791477778912196, 11.05961554403169878 ) ) ;
#70224=CARTESIAN_POINT ( 'NONE',  ( -101.1710158166120692, -25.07377586470730790, 7.416935156559355313 ) ) ;
#70226=B_SPLINE_CURVE_WITH_KNOTS ( 'NONE', 3,
 ( #51160, #43055, #81107, #35930 ),
 .UNSPECIFIED., .F., .F.,
 ( 4, 4 ),
 ( 0.6302359605503721207, 0.6392423918224876545 ),
 .UNSPECIFIED. ) ;
#70227=CARTESIAN_POINT ( 'NONE',  ( -129.5561477353246005, -23.48783264082477729, -1.443836473390078590 ) ) ;
#70228=CARTESIAN_POINT ( 'NONE',  ( -99.52609871227460303, -25.31566080173880451, 4.842596112347664850 ) ) ;
#70229=CARTESIAN_POINT ( 'NONE',  ( -16.62890364678930410, -10.96057169749504645, -1.500000000000002220 ) ) ;
#70231=CARTESIAN_POINT ( 'NONE',  ( 15.56394622224390645, 12.30447529683395125, -1.500000000000002220 ) ) ;
#70235=CARTESIAN_POINT ( 'NONE',  ( -92.52287095715009002, -24.66019654487200086, 8.947790411086115725 ) ) ;
#70236=CARTESIAN_POINT ( 'NONE',  ( 14.12806351585482112, -15.20395780304818523, 11.49999999999999645 ) ) ;
#70237=LINE ( 'NONE', #39773, #3025 ) ;
#70238=B_SPLINE_CURVE_WITH_KNOTS ( 'NONE', 3,
 ( #38018, #75568, #46646, #98909 ),
 .UNSPECIFIED., .F., .F.,
 ( 4, 4 ),
 ( 0.5691783989504385355, 0.5701791459912038951 ),
 .UNSPECIFIED. ) ;
#70239=CARTESIAN_POINT ( 'NONE',  ( -40.52287095715005449, -24.99132157543166244, 2.256160258750667502 ) ) ;
#70240=CARTESIAN_POINT ( 'NONE',  ( 15.15630024635751383, 17.02982414992789018, 11.49999999999999645 ) ) ;
#70241=ORIENTED_EDGE ( 'NONE', *, *, #32854, .T. ) ;
#70242=CARTESIAN_POINT ( 'NONE',  ( -69.59707441095807212, -23.96119346886880308, -0.6495511937832122440 ) ) ;
#70244=ORIENTED_EDGE ( 'NONE', *, *, #4063, .F. ) ;
#70245=CARTESIAN_POINT ( 'NONE',  ( 15.73562052650688514, -12.66937975264744587, -1.500000000000002220 ) ) ;
#70248=EDGE_LOOP ( 'NONE', ( #53873, #87424, #74360, #56227 ) ) ;
#70250=VECTOR ( 'NONE', #61272, 1000.000000000000114 ) ;
#70252=CARTESIAN_POINT ( 'NONE',  ( 7.980177114813061579, 21.45908683785374649, -1.500000000000002220 ) ) ;
#70253=CARTESIAN_POINT ( 'NONE',  ( -51.29636648399702636, -25.27420710014245131, 3.969959656738967446 ) ) ;
#70254=CARTESIAN_POINT ( 'NONE',  ( 15.40532884848888884, -15.22192433072940609, -1.500000000000002220 ) ) ;
#70255=CARTESIAN_POINT ( 'NONE',  ( -99.64934318012689118, -25.31535474791540707, 4.927356294767410105 ) ) ;
#70256=CARTESIAN_POINT ( 'NONE',  ( 17.12911088700535700, -11.98135219954639830, 11.49999999999999645 ) ) ;
#70257=VERTEX_POINT ( 'NONE', #81377 ) ;
#70258=CARTESIAN_POINT ( 'NONE',  ( -107.6228709571500701, -24.33927499327855415, 9.819080762295817166 ) ) ;
#70259=CARTESIAN_POINT ( 'NONE',  ( -69.15592802969443653, -25.31612547948029146, 5.438241754530615424 ) ) ;
#70260=CARTESIAN_POINT ( 'NONE',  ( -14.94409825380703616, 16.19114737329946507, 11.49999999999998934 ) ) ;
#70263=AXIS2_PLACEMENT_3D ( 'NONE', #32908, #25283, #63378 ) ;
#70265=CARTESIAN_POINT ( 'NONE',  ( -49.59807878744301490, -25.27344843023344012, 3.677862403480164133 ) ) ;
#70266=CARTESIAN_POINT ( 'NONE',  ( -122.6228709571500701, -24.33927499327855415, 9.819080762295815390 ) ) ;
#70268=CARTESIAN_POINT ( 'NONE',  ( -72.60176318579898691, -23.73791477778911840, 11.05961554403170943 ) ) ;
#70270=VERTEX_POINT ( 'NONE', #97102 ) ;
#70271=VECTOR ( 'NONE', #7284, 1000.000000000000114 ) ;
#70273=ORIENTED_EDGE ( 'NONE', *, *, #25480, .F. ) ;
#70274=CARTESIAN_POINT ( 'NONE',  ( -106.6228709571500843, -24.34917612406837506, 0.1852690917426655925 ) ) ;
#70275=B_SPLINE_CURVE_WITH_KNOTS ( 'NONE', 3,
 ( #7290, #97284, #12542, #20646, #30634, #61610 ),
 .UNSPECIFIED., .F., .F.,
 ( 4, 2, 4 ),
 ( 0.000000000000000000, 0.001380901958385381172, 0.002761803916770762344 ),
 .UNSPECIFIED. ) ;
#70277=CARTESIAN_POINT ( 'NONE',  ( -36.58683833660532514, -24.34968618360933590, 0.1864209137778783110 ) ) ;
#70278=CARTESIAN_POINT ( 'NONE',  ( -15.50425215161893355, 13.37805140191733777, -1.500000000000002220 ) ) ;
#70279=ADVANCED_FACE ( 'NONE', ( #42831 ), #73761, .T. ) ;
#70280=ORIENTED_EDGE ( 'NONE', *, *, #19652, .T. ) ;
#70281=LINE ( 'NONE', #47947, #91429 ) ;
#70282=B_SPLINE_CURVE_WITH_KNOTS ( 'NONE', 3,
 ( #75215, #66143, #43783, #19434, #89452, #49911, #34673, #42307, #35174, #73236, #36658, #13306, #82825, #44286, #74710, #97060, #27563, #3729, #51395, #65643, #58021, #36168, #96557, #27058, #50399, #66644, #67133, #29039, #82333, #81341, #11822, #12809, #67624, #98044, #98543, #28539, #42793, #73725, #90942, #35671, #4220, #58515, #19930, #50899, #81838, #12311, #4721, #43291, #97557, #28057, #59015, #89947, #20416, #59507 ),
 .UNSPECIFIED., .F., .F.,
 ( 4, 1, 1, 1, 1, 2, 2, 1, 2, 2, 1, 1, 2, 2, 1, 2, 2, 2, 1, 2, 2, 1, 1, 1, 1, 2, 2, 2, 2, 1, 1, 1, 2, 2, 4 ),
 ( 0.000000000000000000, 0.06249999999999557299, 0.09374999999999336642, 0.1093749999999920897, 0.1171874999999916039, 0.1210937499999911876, 0.1249999999999907713, 0.1562499999999895361, 0.1718749999999889255, 0.1874999999999883149, 0.2187499999999874545, 0.2343749999999873157, 0.2421874999999875377, 0.2499999999999877875, 0.3124999999999897304, 0.3437499999999905076, 0.3749999999999912847, 0.4999999999999942268, 0.5624999999999956701, 0.5937499999999965583, 0.6249999999999974465, 0.6874999999999988898, 0.7187499999999996669, 0.7343750000000001110, 0.7421875000000003331, 0.7460937500000005551, 0.7500000000000006661, 0.7812500000000013323, 0.8125000000000018874, 0.8437500000000024425, 0.8593750000000027756, 0.8671875000000028866, 0.8710937500000027756, 0.8750000000000027756, 1.000000000000000000 ),
 .UNSPECIFIED. ) ;
#70285=CARTESIAN_POINT ( 'NONE',  ( 4.546662993595487201, 21.82331882591909178, 11.49999999999998934 ) ) ;
#70286=EDGE_CURVE ( 'NONE', #25620, #48372, #12849, .T. ) ;
#70287=CARTESIAN_POINT ( 'NONE',  ( -70.90788765031213359, -25.16125207327868196, 6.936007712053442020 ) ) ;
#70288=CARTESIAN_POINT ( 'NONE',  ( -27.23878724382540284, -24.61900095434126712, 8.198000781698828732 ) ) ;
#70290=CARTESIAN_POINT ( 'NONE',  ( -111.6228709571500559, -24.65952944569304606, 1.056160979905703901 ) ) ;
#70291=CARTESIAN_POINT ( 'NONE',  ( -29.79716636085243664, -24.63645471362255890, 5.521953888132082433 ) ) ;
#70292=CARTESIAN_POINT ( 'NONE',  ( 13.71216040526616098, 15.69570726272272232, 11.49999999999998934 ) ) ;
#70294=CARTESIAN_POINT ( 'NONE',  ( -116.5228709571500900, -23.73907113217699560, -1.053371485780731254 ) ) ;
#70296=ORIENTED_EDGE ( 'NONE', *, *, #94823, .T. ) ;
#70297=B_SPLINE_SURFACE_WITH_KNOTS ( 'NONE', 3, 1, ( 
 ( #13897, #5797 ),
 ( #91527, #36256 ),
 ( #59600, #99132 ),
 ( #51983, #99623 ),
 ( #28640, #82911 ),
 ( #61605, #44875 ),
 ( #45865, #38236 ),
 ( #6296, #98632 ),
 ( #69192, #75798 ),
 ( #76293, #37256 ),
 ( #29132, #30625 ),
 ( #14397, #68204 ),
 ( #100111, #60606 ),
 ( #30124, #92522 ),
 ( #21505, #90531 ),
 ( #5298, #92026 ),
 ( #22001, #84417 ),
 ( #76781, #7285 ),
 ( #45377, #52983 ),
 ( #22995, #67220 ),
 ( #53984, #44374 ),
 ( #13399, #84911 ),
 ( #43869, #75299 ),
 ( #68705, #36753 ),
 ( #67719, #60107 ),
 ( #91031, #61099 ),
 ( #52481, #182 ),
 ( #71705, #47868 ),
 ( #679, #17409 ),
 ( #15395, #31625 ),
 ( #62591, #48368 ),
 ( #2202, #93516 ),
 ( #24512, #47362 ),
 ( #77784, #77288 ),
 ( #7789, #55991 ),
 ( #86418, #38734 ),
 ( #70694, #78788 ),
 ( #86916, #69701 ),
 ( #46357, #39238 ),
 ( #16395, #63099 ),
 ( #25523, #31124 ),
 ( #24011, #56495 ),
 ( #94027, #63606 ),
 ( #79299, #62097 ),
 ( #15897, #93017 ),
 ( #94528, #70196 ),
 ( #16905, #85921 ),
 ( #9795, #33132 ),
 ( #23495, #54474 ),
 ( #9285, #85411 ),
 ( #40747, #54978 ),
 ( #64111, #55481 ),
 ( #95032, #46860 ),
 ( #8292, #78292 ),
 ( #8799, #39738 ),
 ( #1190, #32126 ),
 ( #40251, #71201 ),
 ( #1695, #32629 ),
 ( #25011, #82674 ),
 ( #33640, #17915 ),
 ( #48873, #44124 ),
 ( #41765, #20762 ),
 ( #95533, #11297 ),
 ( #64620, #44622 ),
 ( #79800, #96035 ),
 ( #51739, #57494 ),
 ( #73208, #90794 ),
 ( #13153, #72709 ),
 ( #10297, #28384 ),
 ( #6051, #75547 ),
 ( #49882, #26529 ),
 ( #65113, #2697 ),
 ( #41254, #36498 ),
 ( #42279, #98388 ),
 ( #67463, #28891 ),
 ( #59344, #36001 ),
 ( #37004, #72208 ),
 ( #21263, #87926 ),
 ( #5551, #67969 ),
 ( #98893, #26019 ),
 ( #88428, #29387 ),
 ( #3206, #66976 ),
 ( #56989, #75051 ),
 ( #97889, #18410 ),
 ( #87416, #59857 ),
 ( #34148, #52238 ),
 ( #49378, #18901 ),
 ( #80813, #83166 ),
 ( #13650, #80309 ),
 ( #10800, #3696 ),
 ( #90292, #62352 ),
 ( #52732, #93277 ),
 ( #99877, #38504 ),
 ( #15661, #8050 ),
 ( #23770, #61856 ),
 ( #92778, #31391 ),
 ( #92282, #83672 ),
 ( #38999, #23261 ),
 ( #77548, #53742 ),
 ( #46125, #54744 ),
 ( #54244, #45623 ),
 ( #30888, #84671 ),
 ( #85680, #15158 ),
 ( #46630, #16159 ),
 ( #38004, #76053 ),
 ( #91290, #69949 ),
 ( #77050, #437 ),
 ( #22757, #76543 ),
 ( #39508, #47128 ),
 ( #68953, #7052 ),
 ( #78043, #8556 ),
 ( #70459, #943 ),
 ( #14152, #60365 ),
 ( #7553, #21759 ),
 ( #14660, #69453 ),
 ( #99394, #45130 ),
 ( #100375, #6555 ),
 ( #37503, #85172 ),
 ( #30385, #68458 ),
 ( #29889, #61358 ),
 ( #60856, #91775 ),
 ( #22258, #53239 ),
 ( #84169, #16658 ),
 ( #33891, #31894 ),
 ( #79564, #72464 ),
 ( #70963, #64876 ),
 ( #80066, #56252 ),
 ( #55248, #41509 ),
 ( #41014, #71468 ),
 ( #32899, #10052 ),
 ( #42020, #47629 ),
 ( #48129, #72965 ),
 ( #71969, #10550 ),
 ( #26278, #87177 ),
 ( #1956, #18657 ),
 ( #1454, #2957 ),
 ( #17665, #55749 ),
 ( #80562, #63870 ),
 ( #94785, #17162 ),
 ( #11056, #88186 ),
 ( #9550, #79057 ),
 ( #32393, #2450 ),
 ( #49632, #95787 ),
 ( #86175, #87682 ),
 ( #48637, #62869 ),
 ( #86674, #33384 ),
 ( #63369, #18166 ),
 ( #64372, #78547 ),
 ( #9051, #40003 ),
 ( #95293, #25777 ),
 ( #56752, #93785 ),
 ( #57255, #94283 ),
 ( #24280, #24766 ),
 ( #40517, #25272 ),
 ( #49138, #3458 ),
 ( #51117, #43995 ),
 ( #42520, #5433 ),
 ( #51618, #27775 ),
 ( #26780, #13035 ),
 ( #12544, #43013 ),
 ( #4452, #82061 ),
 ( #19155, #58725 ),
 ( #11545, #59229 ),
 ( #88685, #81066 ),
 ( #21146, #73956 ),
 ( #74927, #98266 ),
 ( #66361, #58239 ),
 ( #28773, #73458 ),
 ( #13531, #50125 ),
 ( #97287, #34393 ),
 ( #52117, #66855 ),
 ( #90668, #89677 ),
 ( #43510, #97777 ),
 ( #34896, #65371 ),
 ( #65869, #36383 ),
 ( #83040, #20152 ),
 ( #74448, #3951 ),
 ( #90174, #12043 ),
 ( #96788, #67347 ),
 ( #35885, #27284 ),
 ( #59735, #35403 ),
 ( #44503, #4940 ),
 ( #89181, #19651 ),
 ( #50616, #81569 ),
 ( #28271, #96293 ),
 ( #57745, #20648 ),
 ( #82553, #91658 ),
 ( #67848, #315 ),
 ( #7422, #62231 ),
 ( #85044, #83548 ),
 ( #14533, #37389 ),
 ( #75427, #22137 ),
 ( #52609, #99270 ),
 ( #16029, #45508 ),
 ( #23132, #69327 ),
 ( #21636, #5928 ),
 ( #36882, #30763 ),
 ( #29769, #77421 ),
 ( #76423, #76921 ),
 ( #93150, #6928 ),
 ( #60238, #54121 ),
 ( #38374, #37882 ),
 ( #61237, #7924 ),
 ( #100247, #60734 ),
 ( #98768, #15032 ),
 ( #23639, #54610 ),
 ( #68835, #99753 ),
 ( #61735, #14027 ),
 ( #15530, #30257 ),
 ( #92156, #85546 ),
 ( #22632, #53623 ),
 ( #46003, #84547 ),
 ( #29266, #91164 ),
 ( #38872, #75929 ),
 ( #92653, #31260 ),
 ( #45010, #6434 ),
 ( #46494, #68337 ),
 ( #69833, #53121 ),
 ( #84051, #8926 ),
 ( #94662, #39378 ),
 ( #62737, #1828 ),
 ( #88062, #17035 ),
 ( #95168, #40880 ),
 ( #93653, #77919 ),
 ( #8428, #2331 ),
 ( #70835, #49005 ),
 ( #48003, #48506 ),
 ( #33771, #78927 ),
 ( #31768, #25653 ),
 ( #24147, #64246 ),
 ( #79434, #9421 ),
 ( #71840, #32262 ),
 ( #70333, #87050 ),
 ( #64754, #95670 ),
 ( #40385, #86550 ),
 ( #33260, #86050 ),
 ( #56626, #71337 ),
 ( #32763, #26153 ),
 ( #63745, #25142 ),
 ( #55114, #57126 ),
 ( #46995, #24640 ),
 ( #79936, #47498 ),
 ( #87555, #2834 ),
 ( #10425, #18041 ),
 ( #56124, #815 ),
 ( #41386, #78427 ),
 ( #39877, #17540 ),
 ( #9926, #16525 ),
 ( #72342, #1327 ),
 ( #63233, #94156 ),
 ( #55621, #58609 ),
 ( #34772, #51498 ),
 ( #59116, #5309 ),
 ( #28158, #90053 ),
 ( #10932, #20525 ),
 ( #51002, #66243 ),
 ( #41899, #57621 ),
 ( #82431, #12914 ),
 ( #19533, #28653 ),
 ( #43882, #19035 ),
 ( #50010, #50495 ),
 ( #27662, #3342 ),
 ( #74815, #81937 ),
 ( #3831, #36270 ),
 ( #18539, #65742 ),
 ( #96663, #67231 ),
 ( #98145, #59613 ),
 ( #49509, #80443 ),
 ( #72842, #34278 ),
 ( #12421, #97168 ),
 ( #65250, #88562 ),
 ( #66743, #42891 ),
 ( #96174, #26660 ),
 ( #89554, #58123 ),
 ( #81449, #20039 ),
 ( #80944, #11429 ),
 ( #11927, #42406 ),
 ( #27160, #73338 ),
 ( #89060, #73827 ),
 ( #43390, #4328 ),
 ( #35278, #74329 ),
 ( #4820, #35773 ),
 ( #97658, #77303 ),
 ( #13412, #75312 ),
 ( #7804, #53505 ),
 ( #83423, #22511 ),
 ( #21025, #44889 ),
 ( #61111, #7297 ),
 ( #14411, #44386 ),
 ( #45388, #14907 ),
 ( #15409, #194 ),
 ( #61617, #100123 ),
 ( #13911, #76303 ),
 ( #29644, #6802 ),
 ( #75810, #98646 ),
 ( #46370, #38748 ),
 ( #37266, #37758 ),
 ( #30643, #92535 ),
 ( #53996, #69716 ),
 ( #31139, #92039 ),
 ( #84428, #68716 ),
 ( #90545, #68217 ),
 ( #60618, #51994 ),
 ( #29145, #23008 ),
 ( #99633, #6311 ),
 ( #82924, #91539 ),
 ( #53000, #99144 ),
 ( #5809, #36767 ),
 ( #22013, #83930 ),
 ( #67731, #84926 ),
 ( #60118, #91044 ),
 ( #21517, #52494 ),
 ( #30137, #45880 ),
 ( #76796, #38249 ),
 ( #69208, #56506 ),
 ( #54486, #70211 ),
 ( #39251, #46876 ),
 ( #25029, #1709 ),
 ( #32643, #41267 ),
 ( #47379, #62608 ),
 ( #17928, #8813 ),
 ( #33144, #77796 ),
 ( #64127, #62109 ),
 ( #9298, #2215 ),
 ( #692, #95045 ),
 ( #94541, #48885 ),
 ( #23509, #8308 ),
 ( #85934, #25537 ),
 ( #78305, #93030 ),
 ( #2713, #31637 ),
 ( #39749, #85424 ),
 ( #93529, #24023 ),
 ( #79813, #1207 ),
 ( #87430, #10311 ),
 ( #24524, #16406 ),
 ( #72220, #54993 ),
 ( #15909, #70709 ),
 ( #55493, #32138 ),
 ( #63114, #56003 ),
 ( #94040, #47881 ),
 ( #86433, #16918 ),
 ( #78800, #40264 ),
 ( #71215, #63619 ),
 ( #86929, #17422 ),
 ( #48381, #79314 ),
 ( #9809, #40760 ),
 ( #71719, #65625 ),
 ( #96542, #26031 ),
 ( #97540, #10812 ),
 ( #42776, #97044 ),
 ( #43762, #73709 ),
 ( #49894, #66625 ),
 ( #89932, #80828 ),
 ( #4202, #27038 ),
 ( #96049, #95547 ),
 ( #57004, #74212 ),
 ( #35156, #87939 ),
 ( #88939, #66127 ),
 ( #4702, #18423 ),
 ( #64633, #57507 ),
 ( #58007, #18915 ),
 ( #74695, #49393 ),
 ( #19416, #41781 ),
 ( #11311, #80321 ),
 ( #35653, #51375 ),
 ( #11804, #28037 ),
 ( #81821, #88442 ),
 ( #27543, #3710 ),
 ( #58996, #20398 ),
 ( #72721, #3222 ),
 ( #58501, #34159 ),
 ( #26543, #89435 ),
 ( #65126, #42292 ),
 ( #19909, #50883 ),
 ( #50383, #73220 ),
 ( #81322, #12293 ),
 ( #82314, #33653 ),
 ( #34656, #43270 ),
 ( #12792, #67607 ),
 ( #14787, #6686 ),
 ( #90926, #13289 ),
 ( #68594, #44762 ),
 ( #6186, #52874 ),
 ( #15288, #20903 ),
 ( #37137, #44265 ),
 ( #21393, #90428 ),
 ( #7179, #22884 ),
 ( #83809, #76674 ),
 ( #36149, #68099 ),
 ( #37635, #100009 ),
 ( #29517, #46254 ),
 ( #28524, #51878 ),
 ( #99517, #82806 ),
 ( #98524, #30017 ),
 ( #67114, #59994 ),
 ( #76185, #22392 ),
 ( #60498, #59486 ),
 ( #91414, #60988 ),
 ( #30523, #5190 ),
 ( #75195, #5688 ),
 ( #53377, #29022 ),
 ( #75687, #21892 ),
 ( #52371, #36639 ),
 ( #61489, #53872 ),
 ( #83305, #14289 ),
 ( #45753, #38129 ),
 ( #84806, #99021 ),
 ( #91921, #98025 ),
 ( #92414, #45260 ),
 ( #84301, #13789 ),
 ( #69083, #85817 ),
 ( #85306, #40655 ),
 ( #61986, #86316 ),
 ( #16801, #87315 ),
 ( #56394, #16297 ),
 ( #77681, #39134 ),
 ( #23909, #8195 ),
 ( #8700, #17813 ),
 ( #38634, #46759 ),
 ( #17303, #93414 ),
 ( #69598, #2103 ),
 ( #64017, #48268 ),
 ( #23389, #7687 ),
 ( #32027, #86816 ),
 ( #55889, #79198 ),
 ( #47766, #24412 ),
 ( #25420, #76 ),
 ( #9696, #70092 ),
 ( #94425, #33037 ),
 ( #94932, #31021 ),
 ( #92913, #63001 ),
 ( #71606, #575 ),
 ( #31522, #39637 ),
 ( #70593, #54375 ),
 ( #77181, #9187 ),
 ( #62488, #15794 ),
 ( #54877, #47262 ),
 ( #78187, #1086 ),
 ( #93921, #55379 ),
 ( #78681, #40148 ),
 ( #71103, #1593 ),
 ( #32530, #63506 ),
 ( #24911, #41158 ),
 ( #3598, #81210 ),
 ( #89324, #10199 ),
 ( #79702, #72608 ),
 ( #11199, #34041 ),
 ( #65017, #89818 ),
 ( #80714, #56893 ),
 ( #95933, #33535 ),
 ( #50768, #66515 ),
 ( #49283, #72111 ),
 ( #96935, #3107 ),
 ( #50269, #18804 ),
 ( #19795, #35545 ),
 ( #2601, #64521 ),
 ( #11685, #95433 ),
 ( #42172, #97432 ),
 ( #81711, #57895 ),
 ( #26431, #80210 ),
 ( #88833, #10703 ),
 ( #57400, #73109 ),
 ( #27919, #4092 ),
 ( #12183, #58388 ),
 ( #88328, #25920 ),
 ( #34542, #42668 ),
 ( #43160, #87826 ),
 ( #18313, #49780 ),
 ( #65516, #96435 ),
 ( #26927, #48776 ),
 ( #19301, #73602 ),
 ( #35044, #41665 ),
 ( #74102, #58879 ),
 ( #66016, #4597 ),
 ( #27429, #83189 ),
 ( #21781, #90817 ),
 ( #91807, #7075 ),
 ( #43650, #5077 ),
 ( #83696, #36029 ),
 ( #13676, #38025 ),
 ( #22280, #29408 ),
 ( #91312, #37529 ),
 ( #44646, #74587 ),
 ( #75575, #45153 ),
 ( #45645, #30411 ),
 ( #67002, #97915 ),
 ( #68482, #82698 ),
 ( #29910, #52758 ),
 ( #60877, #67490 ),
 ( #76571, #68974 ),
 ( #98412, #37029 ),
 ( #98916, #99416 ),
 ( #84191, #99900 ),
 ( #76078, #51263 ),
 ( #61380, #67991 ),
 ( #60390, #90317 ),
 ( #6576, #28916 ),
 ( #28407, #53264 ),
 ( #14176, #59374 ),
 ( #14682, #59884 ),
 ( #5577, #20288 ),
 ( #20789, #13177 ),
 ( #44148, #82202 ),
 ( #51764, #12686 ),
 ( #75079, #36523 ),
 ( #21289, #52262 ),
 ( #6074, #41921 ),
 ( #48529, #56141 ),
 ( #100398, #72862 ),
 ( #10954, #69974 ),
 ( #9947, #18558 ),
 ( #10445, #49531 ),
 ( #80462, #46147 ),
 ( #22777, #79455 ),
 ( #40900, #46653 ),
 ( #61878, #30911 ),
 ( #3363, #34297 ),
 ( #92307, #25673 ),
 ( #77572, #95689 ),
 ( #53765, #8076 ),
 ( #39023, #26174 ),
 ( #84694, #459 ),
 ( #2350, #25165 ),
 ( #54268, #15183 ),
 ( #77072, #33790 ),
 ( #64267, #7577 ),
 ( #71861, #56645 ),
 ( #64774, #38525 ),
 ( #69480, #15687 ),
 ( #87071, #31415 ),
 ( #92803, #23284 ),
 ( #63765, #85196 ),
 ( #33279, #41406 ),
 ( #57148, #94680 ),
 ( #17562, #95189 ),
 ( #72362, #87576 ),
 ( #18060, #49028 ),
 ( #88085, #79958 ),
 ( #2858, #50030 ),
 ( #28177, #80965 ),
 ( #58631, #52015 ),
 ( #96195, #19555 ),
 ( #35792, #82453 ),
 ( #27182, #82944 ),
 ( #42913, #27681 ),
 ( #13434, #20545 ),
 ( #36292, #74835 ),
 ( #89078, #75333 ),
 ( #11448, #42427 ),
 ( #12935, #58142 ),
 ( #5331, #66762 ),
 ( #50514, #73359 ),
 ( #21045, #44408 ),
 ( #11946, #81960 ),
 ( #67249, #98169 ),
 ( #5830, #97187 ),
 ( #28673, #59634 ),
 ( #65272, #12442 ),
 ( #43412, #34794 ),
 ( #51519, #89576 ),
 ( #26682, #90566 ),
 ( #3853, #74348 ),
 ( #4839, #57641 ),
 ( #88583, #73850 ),
 ( #65764, #81472 ),
 ( #4349, #96680 ),
 ( #20059, #19056 ),
 ( #35300, #66264 ),
 ( #51021, #97681 ),
 ( #59136, #90074 ),
 ( #43902, #23528 ),
 ( #83444, #67750 ),
 ( #38768, #99653 ),
 ( #36787, #53020 ),
 ( #13934, #60638 ),
 ( #77812, #6822 ),
 ( #84944, #30665 ),
 ( #44908, #98668 ),
 ( #29165, #92554 ),
 ( #91559, #69734 ),
 ( #37779, #38269 ),
 ( #75832, #93048 ),
 ( #60140, #45405 ),
 ( #100142, #68735 ),
 ( #22530, #212 ),
 ( #61634, #22035 ),
 ( #91064, #76816 ),
 ( #54506, #85440 ),
 ( #30158, #76322 ),
 ( #62126, #92059 ),
 ( #15927, #77321 ),
 ( #6330, #45899 ),
 ( #99165, #61132 ),
 ( #21537, #46894 ),
 ( #53523, #84446 ),
 ( #23026, #83950 ),
 ( #37285, #31157 ),
 ( #14926, #7315 ),
 ( #54014, #15428 ),
 ( #52514, #69227 ),
 ( #46389, #7822 ),
 ( #68236, #29664 ),
 ( #14431, #26047 ),
 ( #78817, #1222 ),
 ( #40278, #39269 ),
 ( #95563, #79330 ),
 ( #9824, #32658 ),
 ( #2729, #63636 ),
 ( #64143, #33667 ),
 ( #86448, #24040 ),
 ( #70229, #56520 ),
 ( #17941, #40775 ),
 ( #48902, #55513 ),
 ( #56017, #71736 ),
 ( #709, #31655 ),
 ( #8828, #86946 ),
 ( #64648, #72235 ),
 ( #62626, #95065 ),
 ( #94555, #57019 ),
 ( #63130, #17435 ),
 ( #47397, #25551 ),
 ( #71233, #87957 ),
 ( #85951, #93545 ),
 ( #2229, #48396 ),
 ( #33158, #18437 ),
 ( #41280, #78322 ),
 ( #49408, #32156 ),
 ( #79829, #55013 ),
 ( #10325, #8324 ),
 ( #87449, #16423 ),
 ( #39765, #70727 ),
 ( #94056, #24542 ),
 ( #9313, #16933 ),
 ( #47898, #1721 ),
 ( #25042, #11821 ),
 ( #74225, #42791 ),
 ( #4218, #57521 ),
 ( #89451, #43288 ),
 ( #90443, #19928 ),
 ( #96556, #12807 ),
 ( #20414, #67129 ),
 ( #50896, #73722 ),
 ( #42306, #41796 ),
 ( #72739, #51392 ),
 ( #81836, #3239 ),
 ( #35173, #12308 ),
 ( #82330, #34172 ),
 ( #10829, #3728 ),
 ( #66141, #65640 ),
 ( #27056, #20920 ),
 ( #34670, #58020 ),
 ( #88957, #65143 ),
 ( #43780, #26560 ),
 ( #80844, #96067 ),
 ( #28055, #19433 ),
 ( #4718, #50398 ),
 ( #74708, #98042 ),
 ( #88457, #18931 ),
 ( #35669, #49909 ),
 ( #97059, #28537 ),
 ( #5207, #66641 ),
 ( #97554, #59012 ),
 ( #27561, #11329 ),
 ( #58514, #89945 ),
 ( #36165, #80336 ),
 ( #73235, #81339 ),
 ( #59504, #76204 ),
 ( #91428, #6699 ),
 ( #37155, #60013 ),
 ( #7703, #69612 ),
 ( #99036, #68609 ),
 ( #30030, #69097 ),
 ( #14802, #94 ),
 ( #44283, #84821 ),
 ( #61004, #100026 ),
 ( #15305, #38649 ),
 ( #7193, #82822 ),
 ( #31035, #99532 ),
 ( #91938, #21411 ),
 ( #38144, #83826 ),
 ( #62000, #37653 ),
 ( #67622, #68116 ),
 ( #60515, #51895 ),
 ( #13304, #29533 ),
 ( #90939, #92432 ),
 ( #44778, #61505 ),
 ( #36656, #75211 ),
 ( #5703, #84320 ),
 ( #22899, #98540 ),
 ( #53888, #22408 ),
 ( #53392, #29036 ),
 ( #52388, #83322 ),
 ( #46267, #14305 ),
 ( #13803, #92929 ),
 ( #45768, #45277 ),
 ( #30537, #21908 ),
 ( #75703, #77196 ),
 ( #52887, #76693 ),
 ( #6202, #54389 ),
 ( #78201, #55902 ),
 ( #31536, #47780 ),
 ( #55394, #46774 ),
 ( #2115, #86827 ),
 ( #40668, #16816 ),
 ( #9200, #25432 ),
 ( #17317, #8715 ),
 ( #85318, #63517 ),
 ( #17826, #78694 ),
 ( #79211, #48793 ),
 ( #1099, #39149 ),
 ( #48283, #47276 ),
 ( #33053, #24925 ),
 ( #64030, #70607 ),
 ( #32043, #39651 ),
 ( #85831, #79715 ),
 ( #23923, #32545 ),
 ( #64535, #16314 ),
 ( #93429, #15810 ),
 ( #63014, #94439 ),
 ( #10212, #40161 ),
 ( #41169, #94945 ),
 ( #77696, #93937 ),
 ( #86331, #24427 ),
 ( #71116, #23403 ),
 ( #1606, #9711 ),
 ( #71619, #56409 ),
 ( #87328, #72125 ),
 ( #8211, #54893 ),
 ( #2613, #33549 ),
 ( #70107, #590 ),
 ( #62500, #66530 ),
 ( #51274, #57906 ),
 ( #3611, #12697 ),
 ( #65529, #88341 ),
 ( #97445, #4106 ),
 ( #80728, #26446 ),
 ( #35055, #57411 ),
 ( #82215, #73123 ),
 ( #34555, #43665 ),
 ( #27934, #74600 ),
 ( #27445, #18815 ),
 ( #4612, #96947 ),
 ( #35558, #42186 ),
 ( #42680, #58401 ),
 ( #56907, #87841 ),
 ( #95945, #73614 ),
 ( #5092, #58891 ),
 ( #49295, #50783 ),
 ( #36043, #34056 ),
 ( #49795, #25934 ),
 ( #26938, #89834 ),
 ( #95446, #20302 ),
 ( #89339, #10717 ),
 ( #18325, #96446 ),
 ( #11212, #80222 ),
 ( #41679, #3119 ),
 ( #88848, #19313 ),
 ( #66030, #72623 ),
 ( #65032, #50283 ),
 ( #81224, #81724 ),
 ( #11700, #19807 ),
 ( #12196, #43173 ),
 ( #74114, #97927 ),
 ( #21303, #99430 ),
 ( #75094, #91324 ),
 ( #13189, #22791 ),
 ( #28421, #75586 ),
 ( #29925, #37042 ),
 ( #60892, #98933 ),
 ( #52274, #53779 ),
 ( #84205, #37544 ),
 ( #84706, #15197 ),
 ( #29421, #6089 ),
 ( #22294, #38039 ),
 ( #61395, #91819 ),
 ( #21797, #76584 ),
 ( #45659, #7088 ),
 ( #68494, #14190 ),
 ( #46160, #59387 ),
 ( #99912, #67505 ),
 ( #14695, #77088 ),
 ( #30424, #68990 ),
 ( #68003, #7588 ),
 ( #92320, #98425 ),
 ( #28928, #60403 ),
 ( #53276, #52773 ),
 ( #83709, #44162 ),
 ( #76091, #67016 ),
 ( #90329, #6589 ),
 ( #83205, #20804 ),
 ( #51778, #82712 ),
 ( #5592, #45168 ),
 ( #59898, #36537 ),
 ( #90829, #13691 ),
 ( #44662, #100412 ),
 ( #39543, #55282 ),
 ( #55785, #70496 ),
 ( #78581, #86709 ),
 ( #61893, #24313 ),
 ( #63402, #71001 ),
 ( #981, #1492 ),
 ( #47163, #31428 ),
 ( #31933, #86215 ),
 ( #69496, #30923 ),
 ( #77585, #62902 ),
 ( #17199, #48165 ),
 ( #92817, #9089 ),
 ( #93825, #79091 ),
 ( #474, #16696 ),
 ( #15699, #40042 ),
 ( #9593, #40552 ),
 ( #85210, #23297 ),
 ( #47665, #32430 ),
 ( #94319, #71504 ),
 ( #62386, #8090 ),
 ( #38537, #78083 ),
 ( #54283, #93316 ),
 ( #46664, #39038 ),
 ( #24805, #69987 ),
 ( #23807, #54780 ),
 ( #85717, #16195 ),
 ( #8594, #75414 ),
 ( #52596, #30748 ),
 ( #14015, #28760 ),
 ( #69816, #5916 ),
 ( #44995, #59722 ),
 ( #6912, #76906 ),
 ( #92640, #36871 ),
 ( #29249, #90651 ),
 ( #7403, #83533 ),
 ( #23119, #67836 ),
 ( #15514, #60721 ),
 ( #13519, #38360 ),
 ( #44489, #45988 ),
 ( #46478, #14519 ),
 ( #37868, #22617 ),
 ( #60224, #21132 ),
 ( #91148, #76411 ),
 ( #77407, #52102 ),
 ( #61720, #21624 ),
 ( #69314, #85028 ),
 ( #54108, #100234 ),
 ( #29754, #38859 ),
 ( #75915, #68819 ),
 ( #98756, #84534 ),
 ( #7912, #83029 ),
 ( #6421, #61224 ),
 ( #37376, #68321 ),
 ( #99256, #91643 ),
 ( #22124, #53107 ),
 ( #84036, #45495 ),
 ( #99738, #30243 ),
 ( #92142, #53609 ),
 ( #15018, #40865 ),
 ( #71325, #93137 ),
 ( #55606, #32748 ),
 ( #71826, #62217 ),
 ( #9407, #39861 ),
 ( #1311, #47986 ),
 ( #10412, #16015 ),
 ( #32247, #8413 ),
 ( #78914, #48493 ),
 ( #64228, #46983 ),
 ( #801, #23620 ),
 ( #79418, #24131 ),
 ( #1811, #70821 ),
 ( #2319, #87543 ),
 ( #54596, #85530 ),
 ( #63731, #77906 ),
 ( #94141, #18025 ),
 ( #33248, #40370 ),
 ( #31752, #39365 ),
 ( #62721, #48992 ),
 ( #78415, #63218 ),
 ( #79920, #56107 ),
 ( #41373, #95155 ),
 ( #55100, #24627 ),
 ( #86535, #17023 ),
 ( #86036, #70320 ),
 ( #93637, #87036 ),
 ( #16513, #47482 ),
 ( #8912, #94649 ),
 ( #25639, #31246 ),
 ( #25127, #17527 ),
 ( #9912, #56613 ),
 ( #302, #62143 ),
 ( #54524, #23549 ),
 ( #76341, #99183 ),
 ( #37799, #36805 ),
 ( #93066, #76832 ),
 ( #7332, #30173 ),
 ( #85458, #83968 ),
 ( #45423, #15944 ),
 ( #77339, #46909 ),
 ( #38286, #29684 ),
 ( #5849, #6841 ),
 ( #68751, #91574 ),
 ( #67769, #98688 ),
 ( #29184, #60158 ),
 ( #6349, #84464 ),
 ( #91081, #69749 ),
 ( #7840, #15446 ),
 ( #21556, #44927 ),
 ( #37307, #52528 ),
 ( #99668, #231 ),
 ( #61153, #83462 ),
 ( #13950, #75849 ),
 ( #69244, #45918 ),
 ( #100162, #68254 ),
 ( #22055, #60654 ),
 ( #53037, #14447 ),
 ( #92076, #22546 ),
 ( #53537, #14946 ),
 ( #46407, #30679 ),
 ( #61650, #31173 ),
 ( #92568, #23044 ),
 ( #54034, #84960 ),
 ( #38788, #79849 ),
 ( #63148, #77833 ),
 ( #18456, #55028 ),
 ( #78340, #86963 ),
 ( #70245, #10345 ),
 ( #9841, #25060 ),
 ( #726, #16443 ),
 ( #56037, #25568 ),
 ( #17960, #39289 ),
 ( #8340, #1244 ),
 ( #40299, #94074 ),
 ( #24559, #31677 ),
 ( #32175, #55535 ),
 ( #47915, #17452 ),
 ( #72258, #86465 ),
 ( #48418, #48920 ),
 ( #62646, #71250 ),
 ( #40794, #2747 ),
 ( #1739, #87976 ),
 ( #2246, #33688 ),
 ( #26068, #95580 ),
 ( #78835, #70747 ),
 ( #41299, #79348 ),
 ( #16953, #8843 ),
 ( #32678, #93564 ),
 ( #63654, #33178 ),
 ( #64668, #24059 ),
 ( #71755, #64161 ),
 ( #56539, #39785 ),
 ( #87468, #95083 ),
 ( #57040, #9335 ),
 ( #85967, #47414 ),
 ( #94578, #41814 ),
 ( #49931, #27579 ),
 ( #67151, #81358 ),
 ( #4738, #80356 ),
 ( #36184, #66161 ),
 ( #58529, #18952 ),
 ( #35686, #11837 ),
 ( #98059, #43798 ),
 ( #81856, #65165 ),
 ( #51410, #58040 ),
 ( #34689, #49428 ),
 ( #82348, #88478 ),
 ( #96576, #5228 ),
 ( #12829, #96089 ),
 ( #10850, #66662 ),
 ( #73253, #74727 ),
 ( #19448, #50914 ),
 ( #26579, #74242 ),
 ( #34191, #28560 ),
 ( #12331, #50415 ),
 ( #43304, #42810 ),
 ( #3747, #59524 ),
 ( #72760, #89471 ),
 ( #90462, #3255 ),
 ( #73741, #88979 ),
 ( #97574, #20438 ),
 ( #57541, #28075 ),
 ( #4238, #80862 ),
 ( #35190, #97079 ),
 ( #11347, #42322 ),
 ( #65660, #27075 ),
 ( #19945, #59030 ),
 ( #89965, #38667 ),
 ( #53907, #92446 ),
 ( #21927, #31049 ),
 ( #84840, #21429 ),
 ( #52405, #52909 ),
 ( #14820, #83842 ),
 ( #45296, #98561 ),
 ( #30047, #84334 ),
 ( #62018, #61023 ),
 ( #29554, #6218 ),
 ( #61528, #7718 ),
 ( #30553, #22914 ),
 ( #83341, #82841 ),
 ( #13323, #15320 ),
 ( #91953, #44304 ),
 ( #76219, #53410 ),
 ( #46284, #75230 ),
 ( #51913, #44799 ),
 ( #14320, #37176 ),
 ( #68132, #20940 ),
 ( #6716, #29057 ),
 ( #99054, #5724 ),
 ( #77214, #36676 ),
 ( #69632, #45788 ),
 ( #13823, #76709 ),
 ( #67640, #75717 ),
 ( #60532, #60031 ),
 ( #91445, #110 ),
 ( #37669, #68628 ),
 ( #90959, #7210 ),
 ( #38160, #99547 ),
 ( #22425, #69115 ),
 ( #100042, #71633 ),
 ( #39667, #63534 ),
 ( #55919, #41184 ),
 ( #85338, #25449 ),
 ( #71132, #9728 ),
 ( #56424, #48806 ),
 ( #48297, #23421 ),
 ( #79730, #9216 ),
 ( #62518, #31554 ),
 ( #24442, #72140 ),
 ( #87343, #10227 ),
 ( #8228, #78220 ),
 ( #1119, #92945 ),
 ( #54404, #8730 ),
 ( #93447, #33069 ),
 ( #85850, #2133 ),
 ( #77716, #15824 ),
 ( #46791, #24941 ),
 ( #70624, #94460 ),
 ( #17844, #47795 ),
 ( #2627, #64046 ),
 ( #608, #1626 ),
 ( #54907, #93954 ),
 ( #39167, #33569 ),
 ( #78710, #55412 ),
 ( #79228, #32057 ),
 ( #86840, #70123 ),
 ( #63032, #32558 ),
 ( #40683, #94961 ),
 ( #23940, #17336 ),
 ( #16330, #47294 ),
 ( #86351, #16834 ),
 ( #40179, #58905 ),
 ( #96960, #80238 ),
 ( #66548, #73136 ),
 ( #43676, #3626 ),
 ( #65046, #26461 ),
 ( #11227, #95963 ),
 ( #49307, #56921 ),
 ( #64547, #27460 ),
 ( #4622, #87854 ),
 ( #97459, #11716 ),
 ( #88863, #18340 ),
 ( #74129, #72640 ),
 ( #34574, #57425 ),
 ( #42694, #10731 ),
 ( #41696, #19330 ),
 ( #3133, #19820 ),
 ( #58419, #89847 ),
 ( #42204, #73629 ),
 ( #20315, #95460 ),
 ( #18830, #89353 ),
 ( #34074, #50301 ),
 ( #88354, #50797 ),
 ( #49811, #12710 ),
 ( #81736, #65543 ),
 ( #12210, #96461 ),
 ( #80743, #51288 ),
 ( #25950, #4120 ),
 ( #82229, #74614 ),
 ( #26950, #57922 ),
 ( #43187, #35570 ),
 ( #27950, #5108 ),
 ( #81237, #35071 ),
 ( #66044, #76600 ),
 ( #6607, #83726 ),
 ( #84726, #97941 ),
 ( #69006, #36552 ),
 ( #13205, #53794 ),
 ( #99932, #7105 ),
 ( #37055, #46175 ),
 ( #30445, #67520 ),
 ( #98442, #68020 ),
 ( #92336, #83225 ),
 ( #45182, #98947 ),
 ( #28944, #28436 ),
 ( #14206, #38053 ),
 ( #75112, #61411 ),
 ( #68511, #22810 ),
 ( #59399, #82727 ),
 ( #59913, #15216 ),
 ( #21317, #36058 ),
 ( #77104, #44179 ),
 ( #52289, #67033 ),
 ( #76105, #84222 ),
 ( #99443, #90347 ),
 ( #90846, #20819 ),
 ( #14710, #13708 ),
 ( #51794, #5608 ),
 ( #44680, #29437 ),
 ( #75600, #6105 ),
 ( #60416, #53292 ),
 ( #91338, #21814 ),
 ( #37558, #29939 ),
 ( #52790, #60910 ),
 ( #91837, #22314 ),
 ( #45677, #70511 ),
 ( #94841, #63422 ),
 ( #1511, #79115 ),
 ( #70006, #62921 ),
 ( #9107, #86730 ),
 ( #54798, #78599 ),
 ( #71021, #56310 ),
 ( #24332, #32954 ),
 ( #48184, #85228 ),
 ( #39561, #40571 ),
 ( #17218, #8614 ),
 ( #46682, #71523 ),
 ( #77604, #8111 ),
 ( #1001, #87229 ),
 ( #2010, #63930 ),
 ( #23316, #93333 ),
 ( #16216, #7605 ),
 ( #38558, #23825 ),
 ( #39056, #55804 ),
 ( #29622, #30941 ),
 ( #15715, #16716 ),
 ( #31949, #85733 ),
 ( #17726, #54300 ),
 ( #93842, #492 ),
 ( #47182, #92833 ),
 ( #25332, #78101 ),
 ( #86234, #9610 ),
 ( #69514, #55302 ),
 ( #40066, #48694 ),
 ( #47684, #61908 ),
 ( #32448, #31443 ),
 ( #62406, #94340 ),
 ( #24827, #66422 ),
 ( #81622, #88743 ),
 ( #50180, #96843 ),
 ( #3509, #33443 ),
 ( #34453, #4004 ),
 ( #4507, #89737 ),
 ( #81119, #73512 ),
 ( #27336, #41574 ),
 ( #89235, #11600 ),
 ( #19704, #26339 ),
 ( #35454, #97345 ),
 ( #57312, #96346 ),
 ( #50677, #12096 ),
 ( #27831, #11108 ),
 ( #43066, #74012 ),
 ( #20205, #18226 ),
 ( #57799, #49195 ),
 ( #34947, #42078 ),
 ( #58786, #79617 ),
 ( #42577, #95348 ),
 ( #19212, #10109 ),
 ( #41068, #88243 ),
 ( #80120, #72522 ),
 ( #18710, #10609 ),
 ( #73023, #72025 ),
 ( #2509, #3015 ),
 ( #64432, #95846 ),
 ( #25833, #56808 ),
 ( #87740, #65429 ),
 ( #26834, #33951 ),
 ( #64930, #65923 ),
 ( #49689, #80620 ),
 ( #58297, #83605 ),
 ( #36439, #53180 ),
 ( #51173, #67405 ),
 ( #98326, #84111 ),
 ( #91715, #37938 ),
 ( #60795, #22195 ),
 ( #43564, #14595 ),
 ( #14091, #98830 ),
 ( #21697, #74500 ),
 ( #5989, #45068 ),
 ( #45567, #12602 ),
 ( #60297, #90731 ),
 ( #52171, #29325 ),
 ( #61295, #66912 ),
 ( #83101, #59284 ),
 ( #29824, #92221 ),
 ( #75988, #76484 ),
 ( #51678, #4994 ),
 ( #13592, #5490 ),
 ( #6990, #90231 ),
 ( #82118, #97833 ),
 ( #68887, #35943 ),
 ( #99812, #6495 ),
 ( #44057, #37446 ),
 ( #28328, #28833 ),
 ( #82611, #20705 ),
 ( #13090, #30319 ),
 ( #59798, #44559 ),
 ( #74990, #21204 ),
 ( #68397, #75486 ),
 ( #36939, #67910 ),
 ( #52670, #91221 ),
 ( #99329, #93718 ),
 ( #86113, #71401 ),
 ( #15099, #55685 ),
 ( #882, #39941 ),
 ( #86614, #78992 ),
 ( #78488, #70393 ),
 ( #84611, #46065 ),
 ( #23200, #31835 ),
 ( #9490, #17100 ),
 ( #76984, #8988 ),
 ( #8494, #40451 ),
 ( #77485, #62804 ),
 ( #61793, #70902 ),
 ( #1887, #32832 ),
 ( #63809, #55185 ),
 ( #7987, #24705 ),
 ( #24211, #22693 ),
 ( #38936, #54185 ),
 ( #53680, #69891 ),
 ( #16590, #54677 ),
 ( #48064, #7481 ),
 ( #47568, #63300 ),
 ( #92712, #38438 ),
 ( #1393, #47066 ),
 ( #69391, #32328 ),
 ( #94219, #62293 ),
 ( #376, #100310 ),
 ( #30828, #85109 ),
 ( #31324, #15593 ),
 ( #46557, #93217 ),
 ( #23705, #85608 ),
 ( #16096, #77980 ),
 ( #39444, #18106 ),
 ( #96237, #64817 ),
 ( #5737, #40945 ),
 ( #51926, #79501 ),
 ( #9989, #11487 ),
 ( #82855, #80502 ),
 ( #3402, #88624 ),
 ( #25713, #56187 ),
 ( #56692, #13340 ),
 ( #72406, #57193 ),
 ( #44318, #50067 ),
 ( #75246, #90478 ),
 ( #49071, #18595 ),
 ( #33829, #49570 ),
 ( #41448, #65315 ),
 ( #88127, #71905 ),
 ( #10994, #36691 ),
 ( #96723, #34338 ),
 ( #80000, #87623 ),
 ( #26720, #10487 ),
 ( #94723, #2900 ),
 ( #95731, #25209 ),
 ( #65805, #87112 ),
 ( #57681, #26220 ),
 ( #3897, #19095 ),
 ( #34836, #41961 ),
 ( #72905, #81007 ),
 ( #17605, #48577 ),
 ( #95230, #42464 ),
 ( #2390, #73402 ),
 ( #27224, #59540 ),
 ( #33320, #64309 ),
 ( #20953, #98577 ),
 ( #99560, #62031 ),
 ( #85349, #92957 ),
 ( #100053, #83354 ),
 ( #69642, #76233 ),
 ( #52924, #67658 ),
 ( #120, #6233 ),
 ( #54414, #60547 ),
 ( #38677, #52423 ),
 ( #31059, #29072 ),
 ( #14834, #7731 ),
 ( #60046, #23431 ),
 ( #91968, #90974 ),
 ( #77223, #75732 ),
 ( #6730, #29569 ),
 ( #45800, #21442 ),
 ( #13839, #22438 ),
 ( #15834, #46805 ),
 ( #77724, #61539 ),
 ( #14333, #45311 ),
 ( #8239, #44813 ),
 ( #30063, #21938 ),
 ( #37683, #69131 ),
 ( #37189, #61036 ),
 ( #30568, #46295 ),
 ( #68643, #38170 ),
 ( #92457, #68145 ),
 ( #99070, #91462 ),
 ( #76722, #84853 ),
 ( #83856, #53421 ),
 ( #22931, #84351 ),
 ( #7223, #53920 ),
 ( #15333, #70634 ),
 ( #33579, #33079 ),
 ( #87868, #63551 ),
 ( #23951, #48310 ),
 ( #79239, #49320 ),
 ( #18353, #47804 ),
 ( #78229, #79745 ),
 ( #32068, #48819 ),
 ( #54918, #31567 ),
 ( #39178, #71645 ),
 ( #55423, #9738 ),
 ( #64557, #94471 ),
 ( #25962, #10236 ),
 ( #85863, #70132 ),
 ( #41199, #1636 ),
 ( #621, #86362 ),
 ( #16339, #63043 ),
 ( #93963, #2146 ),
 ( #80253, #95476 ),
 ( #2640, #47306 ),
 ( #94969, #87358 ),
 ( #72152, #40693 ),
 ( #64058, #56934 ),
 ( #71145, #8740 ),
 ( #78723, #32570 ),
 ( #56435, #24955 ),
 ( #55929, #62528 ),
 ( #25458, #24457 ),
 ( #93458, #17855 ),
 ( #39679, #1130 ),
 ( #16846, #9227 ),
 ( #40190, #86850 ),
 ( #17348, #58919 ),
 ( #59415, #3146 ),
 ( #26961, #81751 ),
 ( #36076, #66054 ),
 ( #97954, #51303 ),
 ( #57439, #41709 ),
 ( #12722, #73642 ),
 ( #10744, #57936 ),
 ( #96974, #42708 ),
 ( #74629, #28451 ),
 ( #4634, #5124 ),
 ( #88875, #89364 ),
 ( #67046, #72650 ),
 ( #65558, #43200 ),
 ( #18845, #35083 ),
 ( #4134, #26475 ),
 ( #19346, #27474 ),
 ( #27964, #58431 ),
 ( #19832, #34087 ),
 ( #90360, #12223 ),
 ( #74141, #50810 ),
 ( #20833, #35587 ),
 ( #66561, #51810 ),
 ( #65060, #97473 ),
 ( #82243, #89862 ),
 ( #20332, #43691 ),
 ( #95976, #88367 ),
 ( #49826, #80759 ),
 ( #11240, #42216 ),
 ( #73150, #3640 ),
 ( #34586, #96473 ),
 ( #50312, #81248 ),
 ( #11730, #69530 ),
 ( #37072, #60924 ),
 ( #21330, #38066 ),
 ( #61922, #13 ),
 ( #38573, #14725 ),
 ( #68036, #84742 ),
 ( #22327, #92851 ),
 ( #98961, #83241 ),
 ( #30955, #29450 ),
 ( #91853, #14219 ),
 ( #15230, #82740 ),
 ( #28957, #13223 ),
 ( #46188, #45195 ),
 ( #44195, #60430 ),
 ( #59930, #6120 ),
 ( #75614, #45691 ),
 ( #76614, #77117 ),
 ( #91354, #53305 ),
 ( #7624, #75130 ),
 ( #21829, #7118 ),
 ( #90858, #6621 ),
 ( #52306, #69023 ),
 ( #67536, #23329 ),
 ( #99947, #52806 ),
 ( #68526, #5622 ),
 ( #30460, #83739 ),
 ( #84238, #37575 ),
 ( #36566, #99456 ),
 ( #61425, #98457 ),
 ( #13724, #92351 ),
 ( #53810, #22823 ),
 ( #29957, #44695 ),
 ( #76123, #94857 ),
 ( #24844, #1524 ),
 ( #2528, #15729 ),
 ( #87247, #54811 ),
 ( #31460, #72042 ),
 ( #8131, #9625 ),
 ( #40080, #41088 ),
 ( #8628, #32463 ),
 ( #93347, #40587 ),
 ( #33458, #64448 ),
 ( #10124, #86746 ),
 ( #39575, #56325 ),
 ( #54314, #70528 ),
 ( #1016, #17741 ),
 ( #95363, #31962 ),
 ( #63438, #86250 ),
 ( #16233, #46698 ),
 ( #77618, #25347 ),
 ( #55818, #39069 ),
 ( #2032, #78615 ),
 ( #70021, #17234 ),
 ( #48710, #507 ),
 ( #79631, #94358 ),
 ( #9123, #62423 ),
 ( #23839, #85240 ),
 ( #85749, #16729 ),
 ( #47197, #62935 ),
 ( #78116, #93855 ),
 ( #24349, #48201 ),
 ( #55316, #47696 ),
 ( #71034, #79131 ),
 ( #71537, #32971 ),
 ( #63948, #27849 ),
 ( #33965, #50198 ),
 ( #57823, #41592 ),
 ( #34472, #88763 ),
 ( #43089, #19234 ),
 ( #11619, #58806 ),
 ( #19722, #11126 ),
 ( #87756, #65943 ),
 ( #43582, #12623 ),
 ( #81140, #65446 ),
 ( #81644, #97368 ),
 ( #20227, #58317 ),
 ( #42598, #35475 ),
 ( #4526, #66443 ),
 ( #5014, #82138 ),
 ( #3528, #73042 ),
 ( #51196, #89755 ),
 ( #3030, #74523 ),
 ( #35963, #66933 ),
 ( #26854, #25849 ),
 ( #56825, #26354 ),
 ( #57328, #73532 ),
 ( #18241, #49210 ),
 ( #80139, #89255 ),
 ( #42095, #10630 ),
 ( #72536, #96365 ),
 ( #4023, #64948 ),
 ( #95861, #88258 ),
 ( #34969, #96865 ),
 ( #18732, #49710 ),
 ( #80642, #27356 ),
 ( #50696, #12115 ),
 ( #74033, #77003 ),
 ( #92239, #53703 ),
 ( #13114, #83122 ),
 ( #6009, #97851 ),
 ( #28345, #13612 ),
 ( #36457, #37958 ),
 ( #90749, #7011 ),
 ( #82629, #90252 ),
 ( #59309, #29847 ),
 ( #68910, #20726 ),
 ( #45087, #45587 ),
 ( #51696, #44078 ),
 ( #5508, #6515 ),
 ( #59816, #98849 ),
 ( #75011, #7507 ),
 ( #52690, #29345 ),
 ( #61315, #15120 ),
 ( #91738, #22712 ),
 ( #75508, #76011 ),
 ( #84629, #67425 ),
 ( #99835, #99349 ),
 ( #60814, #30342 ),
 ( #60315, #98349 ),
 ( #46084, #38459 ),
 ( #67930, #21223 ),
 ( #91245, #28853 ),
 ( #52194, #68415 ),
 ( #22217, #21716 ),
 ( #44580, #83629 ),
 ( #53199, #36962 ),
 ( #14112, #37467 ),
 ( #84129, #14618 ),
 ( #76503, #8513 ),
 ( #31855, #54697 ),
 ( #48597, #25229 ),
 ( #47086, #16115 ),
 ( #94743, #9510 ),
 ( #56207, #32853 ),
 ( #23220, #24725 ),
 ( #55204, #79013 ),
 ( #62824, #85632 ),
 ( #79520, #87135 ),
 ( #78002, #39465 ),
 ( #17625, #40470 ),
 ( #46581, #10010 ),
 ( #1912, #71420 ),
 ( #70417, #69413 ),
 ( #63831, #69911 ),
 ( #395, #900 ),
 ( #63323, #93738 ),
 ( #77505, #54204 ),
 ( #32346, #9010 ),
 ( #39961, #100330 ),
 ( #24233, #31348 ),
 ( #30846, #86135 ),
 ( #78506, #16610 ),
 ( #62312, #61813 ),
 ( #92734, #85128 ),
 ( #70923, #15614 ),
 ( #47588, #1412 ),
 ( #8007, #38955 ),
 ( #94241, #55707 ),
 ( #86634, #17118 ),
 ( #93237, #23726 ),
 ( #48088, #33851 ),
 ( #19614, #82021 ),
 ( #73420, #4408 ),
 ( #41467, #2412 ),
 ( #89141, #64839 ),
 ( #42487, #11014 ),
 ( #51081, #87642 ),
 ( #97247, #25740 ),
 ( #58688, #3917 ),
 ( #95748, #34854 ),
 ( #71928, #26240 ),
 ( #11505, #58199 ),
 ( #65334, #95249 ),
 ( #96255, #65822 ),
 ( #27738, #96747 ),
 ( #89635, #35360 ),
 ( #2919, #26739 ),
 ( #81533, #33340 ),
 ( #42975, #88645 ),
 ( #57701, #64332 ),
 ( #50577, #49091 ),
 ( #80522, #57213 ),
 ( #19115, #56710 ),
 ( #18126, #50088 ),
 ( #20119, #66321 ),
 ( #40968, #27243 ),
 ( #80023, #10507 ),
 ( #72426, #88146 ),
 ( #18616, #12007 ),
 ( #49589, #81028 ),
 ( #41982, #73910 ),
 ( #72923, #3423 ),
 ( #34357, #83003 ),
 ( #44967, #44466 ),
 ( #67305, #99712 ),
 ( #29727, #83506 ),
 ( #30216, #61199 ),
 ( #75391, #52076 ),
 ( #68294, #84007 ),
 ( #6887, #75892 ),
 ( #36850, #92118 ),
 ( #91617, #53080 ),
 ( #13990, #60196 ),
 ( #22589, #74409 ),
 ( #45469, #12995 ),
 ( #60695, #68795 ),
 ( #76385, #14494 ),
 ( #13494, #53584 ),
 ( #37839, #43958 ),
 ( #74893, #5888 ),
 ( #6396, #67813 ),
 ( #98735, #90134 ),
 ( #21598, #37353 ),
 ( #12505, #52572 ),
 ( #21105, #98228 ),
 ( #43470, #4901 ),
 ( #99225, #29228 ),
 ( #5394, #35847 ),
 ( #66821, #28736 ),
 ( #82513, #51578 ),
 ( #91125, #97741 ),
 ( #28233, #59195 ),
 ( #20611, #59696 ),
 ( #22096, #36348 ),
 ( #90629, #270 ),
 ( #23092, #24599 ),
 ( #85003, #93606 ),
 ( #25100, #46451 ),
 ( #16483, #31726 ),
 ( #76874, #54081 ),
 ( #62691, #32214 ),
 ( #7378, #38332 ),
 ( #92611, #24102 ),
 ( #77381, #85503 ),
 ( #69289, #94619 ),
 ( #39330, #15984 ),
 ( #47455, #63191 ),
 ( #40339, #78381 ),
 ( #30725, #15487 ),
 ( #39832, #94114 ),
 ( #86506, #86008 ),
 ( #8887, #55576 ),
 ( #70792, #71293 ),
 ( #32718, #1780 ),
 ( #54563, #7881 ),
 ( #46956, #14994 ),
 ( #69792, #38832 ),
 ( #55073, #31218 ),
 ( #63702, #62188 ),
 ( #23593, #84509 ),
 ( #16990, #45962 ),
 ( #1285, #93113 ),
 ( #100205, #77878 ),
 ( #8383, #70292 ),
 ( #61692, #773 ),
 ( #47958, #78879 ),
 ( #9380, #96614 ),
 ( #73781, #88017 ),
 ( #27113, #65700 ),
 ( #66201, #95123 ),
 ( #41342, #87516 ),
 ( #96130, #17999 ),
 ( #42852, #33728 ),
 ( #95626, #4280 ),
 ( #58082, #35230 ),
 ( #88516, #79890 ),
 ( #89015, #57580 ),
 ( #19491, #2789 ),
 ( #3301, #18992 ),
 ( #64709, #72795 ),
 ( #50452, #81401 ),
 ( #97121, #18495 ),
 ( #11881, #56074 ),
 ( #87006, #25613 ),
 ( #56581, #17497 ),
 ( #49468, #48462 ),
 ( #79392, #9881 ),
 ( #49970, #71797 ),
 ( #40832, #26112 ),
 ( #72295, #2290 ),
 ( #33220, #48959 ),
 ( #64201, #10383 ),
 ( #57082, #80399 ),
 ( #10889, #41856 ),
 ( #34233, #65207 ),
 ( #26617, #80898 ),
 ( #11385, #42363 ),
 ( #73294, #3789 ),
 ( #34726, #90010 ),
 ( #75270, #19992 ),
 ( #43345, #82880 ),
 ( #14364, #91489 ),
 ( #21968, #21470 ),
 ( #74769, #5266 ),
 ( #99096, #52951 ),
 ( #90502, #82388 ),
 ( #35730, #51952 ),
 ( #74284, #52448 ),
 ( #12372, #76262 ),
 ( #90997, #98103 ),
 ( #60072, #59570 ),
 ( #12867, #28113 ),
 ( #20978, #68669 ),
 ( #89507, #97613 ),
 ( #68170, #43838 ),
 ( #50959, #83881 ),
 ( #13367, #81898 ),
 ( #37219, #66701 ),
 ( #67187, #20483 ),
 ( #5764, #4775 ),
 ( #59073, #51452 ),
 ( #36224, #83379 ),
 ( #27619, #45338 ),
 ( #6755, #28608 ),
 ( #44343, #13868 ),
 ( #36721, #29595 ),
 ( #67685, #98606 ),
 ( #29096, #44839 ),
 ( #75763, #37710 ),
 ( #6261, #60572 ),
 ( #58567, #31091 ),
 ( #53952, #87773 ),
 ( #17758, #70163 ),
 ( #53454, #95379 ),
 ( #62061, #38705 ),
 ( #54948, #72060 ),
 ( #2542, #48727 ),
 ( #54443, #10143 ),
 ( #79645, #41105 ),
 ( #646, #46833 ),
 ( #49229, #61065 ),
 ( #33475, #100080 ),
 ( #64467, #56841 ),
 ( #18255, #84383 ),
 ( #30093, #85377 ),
 ( #15864, #84880 ),
 ( #30595, #92986 ),
 ( #80157, #10646 ),
 ( #41609, #31594 ),
 ( #15361, #25868 ),
 ( #99588, #46326 ),
 ( #77256, #91993 ),
 ( #22464, #14863 ),
 ( #45831, #76749 ),
 ( #7250, #22959 ),
 ( #23461, #7759 ),
 ( #38204, #69160 ),
 ( #77749, #61567 ),
 ( #92491, #69669 ),
 ( #148, #8265 ),
 ( #39203, #62560 ),
 ( #93484, #23976 ),
 ( #87262, #42610 ),
 ( #43597, #59320 ),
 ( #88276, #11632 ),
 ( #34981, #57343 ),
 ( #65461, #4543 ),
 ( #3046, #26869 ),
 ( #43101, #89768 ),
 ( #96879, #26370 ),
 ( #27370, #97379 ),
 ( #97863, #82645 ),
 ( #74045, #66461 ),
 ( #20240, #34484 ),
 ( #82150, #35488 ),
 ( #57836, #80656 ),
 ( #27863, #20739 ),
 ( #64965, #5027 ),
 ( #50708, #51208 ),
 ( #35975, #28359 ),
 ( #58820, #33983 ),
 ( #90264, #89267 ),
 ( #81658, #42114 ),
 ( #12635, #4039 ),
 ( #51707, #66945 ),
 ( #74537, #18745 ),
 ( #12129, #13125 ),
 ( #72552, #81155 ),
 ( #11141, #95876 ),
 ( #96378, #49724 ),
 ( #73057, #3542 ),
 ( #88778, #19245 ),
 ( #50213, #73546 ),
 ( #65959, #19736 ),
 ( #58331, #61827 ),
 ( #100345, #76517 ),
 ( #7023, #84140 ),
 ( #14630, #23233 ),
 ( #29357, #44594 ),
 ( #30861, #91257 ),
 ( #53213, #76023 ),
 ( #6021, #5520 ),
 ( #91750, #84644 ),
 ( #83135, #46096 ),
 ( #92255, #68428 ),
 ( #67436, #53716 ),
 ( #67940, #77023 ),
 ( #60334, #44093 ),
 ( #85145, #21237 ),
 ( #21731, #36976 ),
 ( #22726, #75021 ),
 ( #37974, #7522 ),
 ( #75522, #36473 ),
 ( #15133, #98864 ),
 ( #45597, #14125 ),
 ( #38477, #92749 ),
 ( #83643, #52705 ),
 ( #28866, #61330 ),
 ( #54219, #29858 ),
 ( #68925, #99851 ),
 ( #45102, #98362 ),
 ( #6527, #59828 ),
 ( #37478, #99364 ),
 ( #90762, #30357 ),
 ( #52207, #69427 ),
 ( #60831, #22229 ),
 ( #13622, #79031 ),
 ( #70432, #1427 ),
 ( #63340, #56224 ),
 ( #78520, #63846 ),
 ( #9528, #31363 ),
 ( #24249, #1929 ),
 ( #40485, #93758 ),
 ( #93256, #71439 ),
 ( #46599, #85652 ),
 ( #32874, #94258 ),
 ( #17641, #38972 ),
 ( #24742, #94759 ),
 ( #16132, #16631 ),
 ( #32364, #25250 ),
 ( #919, #55723 ),
 ( #86650, #87153 ),
 ( #77523, #48613 ),
 ( #15634, #23743 ),
 ( #47603, #8022 ),
 ( #69925, #9028 ),
 ( #17138, #62840 ),
 ( #8529, #78017 ),
 ( #39977, #411 ),
 ( #62327, #54718 ),
 ( #31871, #70940 ),
 ( #48105, #47101 ),
 ( #39480, #55222 ),
 ( #86150, #76151 ),
 ( #59961, #37606 ),
 ( #85267, #6151 ),
 ( #36602, #84771 ),
 ( #14753, #67571 ),
 ( #99489, #76644 ),
 ( #15259, #5652 ),
 ( #75162, #68066 ),
 ( #6650, #29480 ),
 ( #60465, #44231 ),
 ( #98990, #91383 ),
 ( #7145, #22853 ),
 ( #40, #38097 ),
 ( #22354, #46215 ),
 ( #98488, #68555 ),
 ( #69051, #38602 ),
 ( #29984, #54342 ),
 ( #90889, #83770 ),
 ( #60955, #28989 ),
 ( #91881, #30985 ),
 ( #77149, #53341 ),
 ( #21860, #75650 ),
 ( #84270, #37102 ),
 ( #45721, #99977 ),
 ( #21364, #52834 ),
 ( #13753, #52338 ),
 ( #14252, #30486 ),
 ( #69561, #61454 ),
 ( #61953, #7653 ),
 ( #83275, #44725 ),
 ( #92879, #92381 ),
 ( #45227, #53840 ),
 ( #23358, #47727 ),
 ( #48230, #94887 ),
 ( #72076, #79161 ),
 ( #62449, #16264 ),
 ( #71570, #63977 ),
 ( #17776, #17267 ),
 ( #9660, #87275 ),
 ( #78643, #31486 ),
 ( #24376, #9149 ),
 ( #33002, #40110 ),
 ( #1555, #48740 ),
 ( #2556, #86776 ),
 ( #55848, #78144 ),
 ( #33493, #93888 ),
 ( #55345, #64480 ),
 ( #79660, #95394 ),
 ( #40615, #39601 ),
 ( #25884, #86277 ),
 ( #71066, #1049 ),
 ( #56856, #15759 ),
 ( #16757, #62960 ),
 ( #47222, #94390 ),
 ( #46724, #10160 ),
 ( #70052, #2063 ),
 ( #32496, #77650 ),
 ( #70553, #24872 ),
 ( #63468, #41119 ),
 ( #25379, #8157 ),
 ( #93377, #538 ),
 ( #56356, #39095 ),
 ( #23864, #54841 ),
 ( #85782, #8659 ),
 ( #31991, #97874 ),
 ( #58836, #66479 ),
 ( #34501, #58348 ),
 ( #50726, #35988 ),
 ( #80171, #20253 ),
 ( #65975, #4557 ),
 ( #51221, #43610 ),
 ( #43114, #18271 ),
 ( #26386, #82164 ),
 ( #57356, #88289 ),
 ( #19258, #66961 ),
 ( #12647, #74553 ),
 ( #3059, #73071 ),
 ( #96392, #87788 ),
 ( #49243, #3555 ),
 ( #18760, #88794 ),
 ( #28372, #95891 ),
 ( #72566, #10662 ),
 ( #41623, #19750 ),
 ( #65474, #89283 ),
 ( #5041, #42624 ),
 ( #34001, #64977 ),
 ( #49741, #96894 ),
 ( #80668, #50229 ),
 ( #11155, #42131 ),
 ( #73562, #81167 ),
 ( #26883, #57854 ),
 ( #81671, #11647 ),
 ( #4052, #27387 ),
 ( #74061, #35503 ),
 ( #89783, #12144 ),
 ( #97393, #34995 ),
 ( #27878, #75038 ),
 ( #67953, #21745 ),
 ( #76529, #52719 ),
 ( #91274, #90279 ),
 ( #46107, #29872 ),
 ( #60843, #83655 ),
 ( #53726, #14137 ),
 ( #98880, #77035 ),
 ( #30370, #7536 ),
 ( #91761, #83153 ),
 ( #38490, #29370 ),
 ( #45116, #22241 ),
 ( #76034, #6542 ),
 ( #21249, #20751 ),
 ( #51720, #99863 ),
 ( #53225, #82660 ),
 ( #37489, #84153 ),
 ( #68938, #67449 ),
 ( #60348, #52223 ),
 ( #68440, #13138 ),
 ( #5533, #99377 ),
 ( #69440, #22742 ),
 ( #84657, #14644 ),
 ( #6036, #36988 ),
 ( #61342, #15144 ),
 ( #45609, #13637 ),
 ( #100357, #98374 ),
 ( #59331, #7035 ),
 ( #37988, #92265 ),
 ( #44109, #36484 ),
 ( #28878, #59840 ),
 ( #44606, #90778 ),
 ( #75533, #1436 ),
 ( #85154, #25257 ),
 ( #55732, #86658 ),
 ( #40997, #15644 ),
 ( #24751, #1939 ),
 ( #55234, #79546 ),
 ( #86160, #93769 ),
 ( #38983, #10037 ),
 ( #48621, #8539 ),
 ( #47612, #56236 ),
 ( #71451, #8032 ),
 ( #62850, #63855 ),
 ( #61840, #16641 ),
 ( #78531, #85662 ),
 ( #421, #69933 ),
 ( #17147, #24259 ),
 ( #9035, #31373 ),
 ( #39988, #94267 ),
 ( #71954, #70948 ),
 ( #39492, #16142 ),
 ( #93263, #32883 ),
 ( #929, #32374 ),
 ( #17651, #63350 ),
 ( #70442, #31879 ),
 ( #46612, #48113 ),
 ( #79041, #94769 ),
 ( #9536, #47114 ),
 ( #40495, #87161 ),
 ( #30874, #92761 ),
 ( #23247, #54229 ),
 ( #77534, #62337 ),
 ( #23750, #54727 ),
 ( #78027, #12033 ),
 ( #81558, #43000 ),
 ( #73447, #50113 ),
 ( #80549, #49619 ),
 ( #27764, #73941 ),
 ( #80049, #20143 ),
 ( #35388, #4439 ),
 ( #88673, #89665 ),
 ( #57238, #81051 ),
 ( #41496, #58229 ),
 ( #82049, #51106 ),
 ( #58714, #34879 ),
 ( #88172, #66351 ),
 ( #42509, #12530 ),
 ( #18641, #2944 ),
 ( #34382, #65856 ),
 ( #96278, #65360 ),
 ( #64862, #64357 ),
 ( #95278, #97276 ),
 ( #3940, #25764 ),
 ( #57731, #96774 ),
 ( #44869, #2435 ),
 ( #11534, #42008 ),
 ( #11043, #33369 ),
 ( #56735, #10535 ),
 ( #72950, #95776 ),
 ( #87668, #18148 ),
 ( #27272, #49122 ),
 ( #33879, #72449 ),
 ( #50605, #26266 ),
 ( #3447, #26766 ),
 ( #89167, #19144 ),
 ( #19640, #21996 ),
 ( #14890, #37739 ),
 ( #75792, #92021 ),
 ( #52977, #99618 ),
 ( #68698, #7784 ),
 ( #16390, #31620 ),
 ( #39232, #83913 ),
 ( #37249, #31117 ),
 ( #30119, #77777 ),
 ( #45858, #77282 ),
 ( #62585, #7279 ),
 ( #60601, #24005 ),
 ( #38729, #76776 ),
 ( #69695, #38231 ),
 ( #61092, #29625 ),
 ( #54973, #84905 ),
 ( #93511, #85914 ),
 ( #69186, #100106 ),
 ( #62091, #46855 ),
 ( #70189, #177 ),
 ( #30619, #6291 ),
 ( #54469, #15892 ),
 ( #46351, #22989 ),
 ( #93011, #22494 ),
 ( #673, #8287 ),
 ( #14391, #68197 ),
 ( #99126, #91522 ),
 ( #61600, #45371 ),
 ( #76288, #6781 ),
 ( #53486, #92516 ),
 ( #84412, #53978 ),
 ( #15389, #23488 ),
 ( #85404, #87411 ),
 ( #17907, #26523 ),
 ( #32624, #47862 ),
 ( #79292, #79794 ),
 ( #40741, #9789 ),
 ( #9279, #8792 ),
 ( #39733, #87921 ),
 ( #3199, #1183 ),
 ( #78285, #33126 ),
 ( #80303, #78783 ),
 ( #40244, #71699 ),
 ( #57487, #65108 ),
 ( #34141, #10291 ),
 ( #63599, #49372 ),
 ( #47356, #94522 ),
 ( #25004, #10795 ),
 ( #48363, #96028 ),
 ( #55475, #18403 ),
 ( #70689, #41759 ),
 ( #32121, #72704 ),
 ( #48867, #63093 ),
 ( #2195, #41247 ),
 ( #26013, #56490 ),
 ( #94021, #71196 ),
 ( #64106, #55986 ),
 ( #88423, #24506 ),
 ( #95027, #86412 ),
 ( #16899, #1688 ),
 ( #86910, #17403 ),
 ( #25516, #72203 ),
 ( #95528, #2691 ),
 ( #33634, #64614 ),
 ( #56983, #5669 ),
 ( #34637, #58481 ),
 ( #81800, #3691 ),
 ( #12275, #36619 ),
 ( #20884, #28020 ),
 ( #42757, #43253 ),
 ( #65606, #81302 ),
 ( #97025, #74193 ),
 ( #67588, #74679 ),
 ( #98505, #13271 ),
 ( #73690, #4686 ),
 ( #89417, #35634 ),
 ( #4186, #27020 ),
 ( #11787, #29002 ),
 ( #66109, #66609 ),
 ( #59468, #90409 ),
 ( #59974, #96524 ),
 ( #57986, #11291 ),
 ( #18895, #51356 ),
 ( #51858, #42272 ),
 ( #44247, #97519 ),
 ( #75175, #98003 ),
 ( #88924, #49876 ),
 ( #82791, #58974 ),
 ( #80808, #35138 ),
 ( #19394, #27524 ),
 ( #19889, #82296 ),
 ( #12774, #73203 ),
 ( #50863, #89913 ),
 ( #50366, #20382 ),
 ( #43744, #5173 ),
 ( #36128, #67098 ),
 ( #28507, #15271 ),
 ( #75664, #39114 ),
 ( #7668, #84283 ),
 ( #76657, #92895 ),
 ( #84785, #14265 ),
 ( #99991, #14767 ),
 ( #85287, #45733 ),
 ( #46231, #15775 ),
 ( #44743, #61471 ),
 ( #61968, #38616 ),
 ( #7161, #58 ),
 ( #69576, #31001 ),
 ( #70067, #46740 ),
 ( #90908, #52353 ),
 ( #23372, #91395 ),
 ( #77664, #54355 ),
 ( #6165, #77164 ),
 ( #38110, #8172 ),
 ( #45241, #69066 ),
 ( #29496, #556 ),
 ( #31502, #21376 ),
 ( #83287, #22868 ),
 ( #76164, #13765 ),
 ( #37117, #6663 ),
 ( #37617, #68077 ),
 ( #22371, #53853 ),
 ( #53355, #29996 ),
 ( #99002, #60479 ),
 ( #21872, #52848 ),
 ( #30499, #83787 ),
 ( #68574, #99500 ),
 ( #60970, #91895 ),
 ( #92394, #23885 ),
 ( #95411, #62980 ),
 ( #79679, #18288 ),
 ( #25898, #33512 ),
 ( #63485, #72585 ),
 ( #56870, #93902 ),
 ( #24391, #94405 ),
 ( #56372, #24888 ),
 ( #86790, #39617 ),
 ( #71585, #25395 ),
 ( #3078, #2078 ),
 ( #78658, #87803 ),
 ( #55868, #10677 ),
 ( #17283, #48246 ),
 ( #55361, #54858 ),
 ( #85798, #2571 ),
 ( #33017, #16278 ),
 ( #79177, #94905 ),
 ( #41137, #63992 ),
 ( #93394, #86292 ),
 ( #9675, #47743 ),
 ( #9167, #62464 ),
 ( #16780, #40126 ),
 ( #80187, #49260 ),
 ( #87292, #41639 ),
 ( #71081, #47239 ),
 ( #10175, #1573 ),
 ( #17790, #32510 ),
 ( #64495, #78163 ),
 ( #8676, #40632 ),
 ( #48753, #70569 ),
 ( #72090, #1065 ),
 ( #32007, #43129 ),
 ( #12161, #82675 ),
 ( #58362, #88305 ),
 ( #89300, #96411 ),
 ( #81688, #26402 ),
 ( #49757, #19768 ),
 ( #26898, #66492 ),
 ( #75052, #90293 ),
 ( #97890, #80684 ),
 ( #95909, #89797 ),
 ( #57870, #36003 ),
 ( #42146, #50742 ),
 ( #11176, #58850 ),
 ( #18775, #13154 ),
 ( #97405, #4067 ),
 ( #27895, #65991 ),
 ( #88808, #73086 ),
 ( #44126, #74079 ),
 ( #3575, #28386 ),
 ( #20266, #51234 ),
 ( #82177, #5055 ),
 ( #66978, #12662 ),
 ( #4572, #43627 ),
 ( #74565, #59345 ),
 ( #34016, #20763 ),
 ( #64992, #57376 ),
 ( #51741, #34517 ),
 ( #65491, #19274 ),
 ( #50246, #81183 ),
 ( #11663, #35521 ),
 ( #42643, #73578 ),
 ( #35014, #96908 ),
 ( #27403, #68460 ),
 ( #61857, #38005 ),
 ( #91291, #7554 ),
 ( #5553, #21760 ),
 ( #52734, #38505 ),
 ( #6556, #54245 ),
 ( #13651, #77052 ),
 ( #98389, #69454 ),
 ( #68955, #53241 ),
 ( #76545, #28892 ),
 ( #60858, #99878 ),
 ( #84673, #14661 ),
 ( #36499, #29388 ),
 ( #83167, #23262 ),
 ( #100377, #30890 ),
 ( #91776, #92780 ),
 ( #60367, #84171 ),
 ( #44624, #61359 ),
 ( #85174, #15662 ),
 ( #75548, #90795 ),
 ( #30386, #45624 ),
 ( #7053, #46631 ),
 ( #83673, #6052 ),
 ( #37504, #92286 ),
 ( #99395, #29890 ),
 ( #67971, #67464 ),
 ( #59859, #46126 ),
 ( #22758, #21264 ),
 ( #22259, #53743 ),
 ( #15159, #52240 ),
 ( #14154, #37005 ),
 ( #45131, #98894 ),
 ( #76055, #54746 ),
 ( #93786, #70460 ),
 ( #56253, #18167 ),
 ( #9551, #41016 ),
 ( #78045, #39001 ),
 ( #25274, #945 ),
 ( #79058, #47631 ),
 ( #87683, #23771 ),
 ( #33385, #62353 ),
 ( #95294, #40519 ),
 ( #64374, #63370 ),
 ( #86676, #71469 ),
 ( #40004, #71970 ),
 ( #39509, #25778 ),
 ( #55249, #70964 ),
 ( #56754, #32901 ),
 ( #77549, #2451 ),
 ( #31895, #32395 ),
 ( #1957, #87178 ),
 ( #24282, #8052 ),
 ( #24768, #69951 ),
 ( #439, #10053 ),
 ( #55750, #31392 ),
 ( #63871, #93279 ),
 ( #1455, #85681 ),
 ( #94284, #16161 ),
 ( #79565, #17164 ),
 ( #48130, #47129 ),
 ( #94786, #8559 ),
 ( #17666, #48639 ),
 ( #62870, #86177 ),
 ( #16661, #78548 ),
 ( #9053, #11058 ),
 ( #58728, #50618 ),
 ( #89678, #96294 ),
 ( #4941, #96789 ),
 ( #10551, #41510 ),
 ( #27285, #66362 ),
 ( #12546, #35886 ),
 ( #4453, #80067 ),
 ( #66857, #65870 ),
 ( #58240, #18658 ),
 ( #35405, #81069 ),
 ( #97779, #43512 ),
 ( #81570, #64878 ),
 ( #51118, #57746 ),
 ( #34395, #49140 ),
 ( #49633, #42022 ),
 ( #12044, #95788 ),
 ( #11546, #90175 ),
 ( #72465, #80563 ),
 ( #20153, #2959 ),
 ( #82062, #89183 ),
 ( #97289, #59230 ),
 ( #74449, #57257 ),
 ( #88686, #72967 ),
 ( #19653, #33892 ),
 ( #26279, #3459 ),
 ( #65373, #43014 ),
 ( #88187, #28272 ),
 ( #26781, #19156 ),
 ( #50126, #27776 ),
 ( #42522, #73459 ),
 ( #3952, #73957 ),
 ( #34897, #45012 ),
 ( #7424, #98770 ),
 ( #60240, #38376 ),
 ( #91660, #14535 ),
 ( #68837, #83042 ),
 ( #30259, #22139 ),
 ( #61239, #67850 ),
 ( #76923, #68340 ),
 ( #82554, #13037 ),
 ( #21148, #99273 ),
 ( #69329, #84549 ),
 ( #74929, #76425 ),
 ( #6436, #100249 ),
 ( #52118, #51621 ),
 ( #6932, #52611 ),
 ( #30766, #15035 ),
 ( #53124, #36385 ),
 ( #22634, #29270 ),
 ( #5930, #20649 ),
 ( #53626, #59737 ),
 ( #61738, #43996 ),
 ( #92159, #5434 ),
 ( #46006, #67348 ),
 ( #98267, #36883 ),
 ( #28774, #90670 ),
 ( #84053, #13532 ),
 ( #29771, #44504 ),
 ( #75429, #91167 ),
 ( #60736, #21638 ),
 ( #83550, #75932 ),
 ( #14030, #37392 ),
 ( #45511, #37884 ),
 ( #99755, #70335 ),
 ( #54123, #48006 ),
 ( #16031, #94665 ),
 ( #62741, #94159 ),
 ( #79438, #24150 ),
 ( #31771, #818 ),
 ( #77423, #9424 ),
 ( #9930, #78430 ),
 ( #1331, #86554 ),
 ( #55117, #71340 ),
 ( #317, #46997 ),
 ( #92655, #85047 ),
 ( #25147, #93152 ),
 ( #40389, #48509 ),
 ( #40884, #46496 ),
 ( #23135, #8929 ),
 ( #39880, #77921 ),
 ( #62233, #31263 ),
 ( #86053, #71844 ),
 ( #87053, #2334 ),
 ( #7926, #8431 ),
 ( #33263, #32265 ),
 ( #93656, #39381 ),
 ( #16528, #15532 ),
 ( #23642, #63749 ),
 ( #38874, #56127 ),
 ( #24643, #70838 ),
 ( #69837, #54612 ),
 ( #63236, #55625 ),
 ( #85548, #17543 ),
 ( #47503, #17039 ),
 ( #78930, #1831 ),
 ( #32766, #4823 ),
 ( #88066, #80446 ),
 ( #96666, #42895 ),
 ( #20043, #27164 ),
 ( #10428, #64757 ),
 ( #95172, #26664 ),
 ( #58126, #58614 ),
 ( #88565, #74332 ),
 ( #89063, #51006 ),
 ( #57624, #49009 ),
 ( #19039, #81940 ),
 ( #66246, #73342 ),
 ( #18543, #50014 ),
 ( #79941, #26157 ),
 ( #12426, #41903 ),
 ( #3345, #43394 ),
 ( #35282, #64250 ),
 ( #19537, #49512 ),
 ( #25656, #34282 ),
 ( #56629, #89558 ),
 ( #50499, #41389 ),
 ( #97171, #72845 ),
 ( #10936, #87558 ),
 ( #27665, #2839 ),
 ( #18045, #72345 ),
 ( #33774, #95673 ),
 ( #57131, #65254 ),
 ( #11432, #4331 ),
 ( #96179, #80948 ),
 ( #81454, #42410 ),
 ( #3835, #34777 ),
 ( #65745, #11931 ),
 ( #73832, #28162 ),
 ( #51503, #91048 ),
 ( #22515, #99637 ),
 ( #30140, #29648 ),
 ( #82928, #13416 ),
 ( #6807, #61114 ),
 ( #98649, #90549 ),
 ( #5812, #37269 ),
 ( #53508, #67735 ),
 ( #75317, #44391 ),
 ( #20528, #53004 ),
 ( #84431, #21521 ),
 ( #44892, #60622 ),
 ( #29149, #92044 ),
 ( #90056, #14911 ),
 ( #91543, #22016 ),
 ( #45885, #82434 ),
 ( #76800, #68221 ),
 ( #60121, #35776 ),
 ( #52498, #83427 ),
 ( #43885, #59617 ),
 ( #66747, #99148 ),
 ( #13915, #97663 ),
 ( #76306, #12917 ),
 ( #75814, #68720 ),
 ( #45391, #36770 ),
 ( #74819, #59120 ),
 ( #67235, #6314 ),
 ( #83935, #14414 ),
 ( #5313, #37763 ),
 ( #36275, #98148 ),
 ( #28656, #21028 ),
 ( #51997, #3101 ),
 ( #69720, #26425 ),
 ( #85427, #70215 ),
 ( #95928, #63117 ),
 ( #57394, #34036 ),
 ( #198, #62611 ),
 ( #8816, #86436 ),
 ( #54489, #88322 ),
 ( #54997, #7301 ),
 ( #24028, #65012 ),
 ( #47884, #84930 ),
 ( #39256, #40267 ),
 ( #16921, #8311 ),
 ( #46373, #71218 ),
 ( #38252, #38751 ),
 ( #696, #18798 ),
 ( #49774, #69211 ),
 ( #23012, #93034 ),
 ( #15913, #100127 ),
 ( #30647, #23514 ),
 ( #77306, #31642 ),
 ( #61621, #15413 ),
 ( #92538, #54000 ),
 ( #7808, #31143 ),
 ( #46880, #78310 ),
 ( #85937, #16409 ),
 ( #62113, #77799 ),
 ( #93532, #47383 ),
 ( #39753, #70712 ),
 ( #1209, #32141 ),
 ( #94042, #24526 ),
 ( #55496, #78802 ),
 ( #9300, #75072 ),
 ( #58381, #58873 ),
 ( #5572, #11194 ),
 ( #82691, #82195 ),
 ( #4590, #90812 ),
 ( #5072, #27424 ),
 ( #89813, #51759 ),
 ( #42166, #43153 ),
 ( #12680, #36517 ),
 ( #35540, #21283 ),
 ( #36021, #67483 ),
 ( #28910, #98406 ),
 ( #50763, #73596 ),
 ( #13172, #20283 ),
 ( #4086, #74097 ),
 ( #96430, #42663 ),
 ( #59878, #89319 ),
 ( #19788, #80706 ),
 ( #51256, #74582 ),
 ( #28402, #35038 ),
 ( #90311, #43644 ),
 ( #20782, #81706 ),
 ( #73104, #27914 ),
 ( #12178, #97425 ),
 ( #44143, #3593 ),
 ( #34537, #66510 ),
 ( #65510, #26919 ),
 ( #57889, #19294 ),
 ( #81204, #88827 ),
 ( #66997, #50264 ),
 ( #97909, #11680 ),
 ( #66009, #96929 ),
 ( #59368, #60872 ),
 ( #31411, #91798 ),
 ( #52751, #14170 ),
 ( #84689, #67986 ),
 ( #84186, #93296 ),
 ( #13668, #21776 ),
 ( #92798, #68477 ),
 ( #44641, #77567 ),
 ( #15177, #8070 ),
 ( #61374, #98910 ),
 ( #76073, #54262 ),
 ( #99894, #75569 ),
 ( #29403, #7070 ),
 ( #45146, #46142 ),
 ( #52257, #39018 ),
 ( #38019, #14677 ),
 ( #15681, #69970 ),
 ( #77066, #46647 ),
 ( #29904, #30403 ),
 ( #455, #83184 ),
 ( #6572, #7571 ),
 ( #53760, #23279 ),
 ( #45640, #60384 ),
 ( #22274, #76564 ),
 ( #69472, #68969 ),
 ( #92302, #85191 ),
 ( #38519, #37523 ),
 ( #22772, #100393 ),
 ( #62368, #30906 ),
 ( #61873, #6068 ),
 ( #37023, #91307 ),
 ( #83690, #99410 ),
 ( #53258, #63387 ),
 ( #86694, #9072 ),
 ( #47650, #86196 ),
 ( #56273, #70983 ),
 ( #49159, #64396 ),
 ( #962, #41530 ),
 ( #56771, #95311 ),
 ( #24788, #33912 ),
 ( #87702, #24299 ),
 ( #55768, #18186 ),
 ( #17180, #72485 ),
 ( #31915, #8579 ),
 ( #87197, #63891 ),
 ( #94805, #2979 ),
 ( #40025, #55265 ),
 ( #48151, #17685 ),
 ( #79075, #9572 ),
 ( #16680, #85700 ),
 ( #16180, #25799 ),
 ( #62887, #80085 ),
 ( #40537, #79583 ),
 ( #10568, #33404 ),
 ( #78564, #64895 ),
 ( #1473, #23790 ),
 ( #54762, #71487 ),
 ( #25293, #2470 ),
 ( #32414, #47147 ),
 ( #1975, #78065 ),
 ( #39526, #70478 ),
 ( #93806, #94301 ),
 ( #32918, #48660 ),
 ( #10073, #41035 ),
 ( #71990, #28290 ),
 ( #26301, #26798 ),
 ( #90190, #89697 ),
 ( #44015, #19670 ),
 ( #11074, #81086 ),
 ( #3972, #95804 ),
 ( #57276, #11562 ),
 ( #57761, #27300 ),
 ( #42041, #89201 ),
 ( #36404, #88704 ),
 ( #65394, #88207 ),
 ( #42540, #66380 ),
 ( #20669, #50635 ),
 ( #51637, #74465 ),
 ( #72986, #18675 ),
 ( #97798, #58257 ),
 ( #49649, #73475 ),
 ( #19173, #34913 ),
 ( #27793, #4958 ),
 ( #82573, #58746 ),
 ( #3475, #96311 ),
 ( #51133, #43529 ),
 ( #59249, #97308 ),
 ( #20172, #66872 ),
 ( #81589, #34413 ),
 ( #65887, #12060 ),
 ( #12565, #43031 ),
 ( #73973, #80581 ),
 ( #50144, #4472 ),
 ( #35421, #82081 ),
 ( #13054, #35903 ),
 ( #96808, #74946 ),
 ( #5452, #54144 ),
 ( #99771, #91181 ),
 ( #29787, #21656 ),
 ( #61756, #75446 ),
 ( #77443, #13551 ),
 ( #6453, #75949 ),
 ( #52134, #84567 ),
 ( #85067, #53143 ),
 ( #76445, #61257 ),
 ( #60754, #92674 ),
 ( #29287, #15553 ),
 ( #45030, #91675 ),
 ( #46514, #22652 ),
 ( #92179, #38395 ),
 ( #60258, #22156 ),
 ( #84069, #14555 ),
 ( #5946, #52629 ),
 ( #7944, #30277 ),
 ( #45526, #23152 ),
 ( #7440, #44522 ),
 ( #99290, #100268 ),
 ( #76944, #68357 ),
 ( #36902, #30787 ),
 ( #98284, #98790 ),
 ( #67365, #53643 ),
 ( #28791, #59756 ),
 ( #6948, #15054 ),
 ( #90688, #37902 ),
 ( #37411, #83565 ),
 ( #14049, #68853 ),
 ( #83057, #46025 ),
 ( #21167, #69350 ),
 ( #67865, #31281 ),
 ( #62759, #24660 ),
 ( #87072, #39896 ),
 ( #40901, #56142 ),
 ( #85567, #63255 ),
 ( #8451, #16546 ),
 ( #62250, #71862 ),
 ( #70859, #47522 ),
 ( #86572, #71359 ),
 ( #17563, #55641 ),
 ( #54634, #47019 ),
 ( #78948, #38895 ),
 ( #24167, #32285 ),
 ( #94176, #40406 ),
 ( #48531, #79457 ),
 ( #9447, #335 ),
 ( #9949, #17056 ),
 ( #48023, #77938 ),
 ( #1847, #78446 ),
 ( #69856, #93174 ),
 ( #32785, #39398 ),
 ( #23661, #1350 ),
 ( #16050, #63766 ),
 ( #8948, #94681 ),
 ( #70352, #25167 ),
 ( #55139, #93677 ),
 ( #836, #31790 ),
 ( #86071, #21481 ),
 ( #31101, #76761 ),
 ( #84890, #39213 ),
 ( #38716, #37230 ),
 ( #68680, #91501 ),
 ( #7261, #52459 ),
 ( #6273, #52961 ),
 ( #21980, #61578 ),
 ( #22971, #23471 ),
 ( #6766, #38215 ),
 ( #54452, #60084 ),
 ( #83893, #92500 ),
 ( #68182, #53465 ),
 ( #75773, #53961 ),
 ( #13878, #77759 ),
 ( #15372, #99600 ),
 ( #14874, #62072 ),
 ( #46335, #14374 ),
 ( #85386, #44850 ),
 ( #46841, #15875 ),
 ( #92004, #30103 ),
 ( #77266, #159 ),
 ( #92995, #7769 ),
 ( #84395, #69678 ),
 ( #8273, #70171 ),
 ( #29108, #91008 ),
 ( #83392, #99108 ),
 ( #29605, #60584 ),
 ( #45350, #76272 ),
 ( #37721, #61076 ),
 ( #30605, #22475 ),
 ( #45842, #69171 ),
 ( #100091, #40228 ),
 ( #63585, #85895 ),
 ( #94507, #87905 ),
 ( #2676, #9771 ),
 ( #24988, #95511 ),
 ( #63076, #18387 ),
 ( #78764, #55965 ),
 ( #49356, #56470 ),
 ( #80286, #25997 ),
 ( #24490, #86892 ),
 ( #71181, #17385 ),
 ( #86396, #8776 ),
 ( #94001, #10780 ),
 ( #47842, #48347 ),
 ( #79277, #17890 ),
 ( #64596, #56969 ),
 ( #87396, #31603 ),
 ( #39714, #33615 ),
 ( #62570, #32102 ),
 ( #41744, #95008 ),
 ( #656, #40725 ),
 ( #16375, #71683 ),
 ( #2180, #93495 ),
 ( #23985, #9264 ),
 ( #70673, #1670 ),
 ( #54957, #1167 ),
 ( #47341, #78264 ),
 ( #55458, #33112 ),
 ( #41232, #16880 ),
 ( #32609, #64090 ),
 ( #48853, #25499 ),
 ( #79778, #10275 ),
 ( #72187, #35119 ),
 ( #72684, #88908 ),
 ( #27509, #4168 ),
 ( #36110, #81785 ),
 ( #3182, #96506 ),
 ( #66092, #57969 ),
 ( #19379, #13257 ),
 ( #27002, #50346 ),
 ( #4669, #51340 ),
 ( #28489, #35619 ),
 ( #18880, #73185 ),
 ( #28000, #20365 ),
 ( #74174, #42742 ),
 ( #43728, #59451 ),
 ( #88405, #11768 ),
 ( #97007, #57472 ),
 ( #58464, #90396 ),
 ( #74662, #12257 ),
 ( #81285, #89399 ),
 ( #49861, #34622 ),
 ( #20870, #73675 ),
 ( #19871, #51841 ),
 ( #43236, #66593 ),
 ( #82281, #65591 ),
 ( #12756, #97505 ),
 ( #5159, #50846 ),
 ( #58957, #82775 ),
 ( #89897, #67079 ),
 ( #97989, #34122 ),
 ( #65094, #96013 ),
 ( #26508, #80792 ),
 ( #11273, #42254 ),
 ( #3674, #3998 ),
 ( #57790, #81112 ),
 ( #35446, #11101 ),
 ( #72019, #96339 ),
 ( #26826, #97336 ),
 ( #66416, #95838 ),
 ( #87734, #49189 ),
 ( #19203, #2501 ),
 ( #33437, #79611 ),
 ( #85848, #50174 ),
 ( #3007, #88737 ),
 ( #12090, #42070 ),
 ( #43059, #65917 ),
 ( #74007, #50668 ),
 ( #81616, #11593 ),
 ( #33943, #64923 ),
 ( #58289, #4501 ),
 ( #49683, #41566 ),
 ( #27825, #95339 ),
 ( #17719, #64424 ),
 ( #26331, #57306 ),
 ( #42569, #88237 ),
 ( #73505, #18701 ),
 ( #72516, #41060 ),
 ( #48688, #34940 ),
 ( #25827, #10102 ),
 ( #96834, #27329 ),
 ( #56802, #18218 ),
 ( #89229, #19697 ),
 ( #80112, #73016 ),
 ( #3503, #80611 ),
 ( #10601, #34446 ),
 ( #65423, #91212 ),
 ( #75475, #84100 ),
 ( #99321, #35935 ),
 ( #14585, #12595 ),
 ( #89729, #44551 ),
 ( #5980, #13082 ),
 ( #45558, #91703 ),
 ( #90723, #37931 ),
 ( #83092, #66905 ),
 ( #67901, #21689 ),
 ( #68879, #98822 ),
 ( #67395, #44050 ),
 ( #20698, #21196 ),
 ( #74493, #52162 ),
 ( #99803, #51670 ),
 ( #28321, #51165 ),
 ( #74980, #29317 ),
 ( #36930, #60289 ),
 ( #37438, #52659 ),
 ( #20199, #82605 ),
 ( #13582, #5483 ),
 ( #36431, #58777 ),
 ( #82112, #22187 ),
 ( #83594, #75978 ),
 ( #53171, #76477 ),
 ( #14081, #43557 ),
 ( #6983, #45059 ),
 ( #97826, #4988 ),
 ( #6487, #68389 ),
 ( #59275, #29814 ),
 ( #90225, #98318 ),
 ( #28824, #59789 ),
 ( #60787, #46548 ),
 ( #69382, #31315 ),
 ( #40442, #38431 ),
 ( #15090, #22685 ),
 ( #30310, #62795 ),
 ( #70894, #53672 ),
 ( #55677, #85599 ),
 ( #86603, #8979 ),
 ( #76977, #61288 ),
 ( #32319, #93209 ),
 ( #92212, #77478 ),
 ( #7471, #54178 ),
 ( #94210, #48053 ),
 ( #24201, #24695 ),
 ( #7978, #8485 ),
 ( #17090, #84604 ),
 ( #63291, #31825 ),
 ( #93709, #1385 ),
 ( #62284, #46058 ),
 ( #38929, #23695 ),
 ( #47558, #54669 ),
 ( #16088, #78983 ),
 ( #55176, #85102 ),
 ( #9482, #100302 ),
 ( #71393, #30819 ),
 ( #47057, #69883 ),
 ( #61785, #92704 ),
 ( #86104, #15584 ),
 ( #23193, #367 ),
 ( #77971, #39435 ),
 ( #70384, #874 ),
 ( #16582, #78478 ),
 ( #39931, #63800 ),
 ( #50058, #25703 ),
 ( #3392, #72395 ),
 ( #73393, #89114 ),
 ( #58170, #87103 ),
 ( #19586, #65304 ),
 ( #95222, #34327 ),
 ( #10985, #96228 ),
 ( #64806, #96712 ),
 ( #64299, #50548 ),
 ( #79990, #95721 ),
 ( #81501, #57671 ),
 ( #11980, #27215 ),
 ( #56681, #26210 ),
 ( #26711, #80997 ),
 ( #49062, #42948 ),
 ( #49561, #1877 ),
 ( #94715, #34827 ),
 ( #80490, #19086 ),
 ( #65797, #32823 ),
 ( #88614, #25200 ),
 ( #40935, #56175 ),
 ( #42454, #11479 ),
 ( #72895, #3888 ),
 ( #17595, #48568 ),
 ( #79493, #87613 ),
 ( #10478, #9981 ),
 ( #71896, #18097 ),
 ( #2381, #2890 ),
 ( #33312, #41438 ),
 ( #33820, #57183 ),
 ( #88117, #18584 ),
 ( #41950, #66291 ),
 ( #75865, #21081 ),
 ( #83983, #68271 ),
 ( #81995, #82978 ),
 ( #35822, #74866 ),
 ( #97219, #14462 ),
 ( #28710, #5369 ),
 ( #37325, #91592 ),
 ( #67789, #99200 ),
 ( #29699, #73884 ),
 ( #44440, #98706 ),
 ( #21572, #66795 ),
 ( #12967, #59671 ),
 ( #59164, #12478 ),
 ( #97714, #53052 ),
 ( #20582, #90601 ),
 ( #52047, #91096 ),
 ( #60669, #22071 ),
 ( #29205, #4382 ),
 ( #35330, #13468 ),
 ( #43447, #27713 ),
 ( #74377, #36323 ),
 ( #58660, #98200 ),
 ( #89608, #75364 ),
 ( #5864, #20087 ),
 ( #51055, #82485 ),
 ( #4875, #28207 ),
 ( #36821, #90108 ),
 ( #67282, #51555 ),
 ( #43934, #60173 ),
 ( #13966, #52544 ),
 ( #6367, #83479 ),
 ( #44942, #24075 ),
 ( #92092, #76357 ),
 ( #47428, #7855 ),
 ( #45443, #61667 ),
 ( #22560, #69260 ),
 ( #38303, #77850 ),
 ( #86479, #1259 ),
 ( #8856, #53553 ),
 ( #6861, #744 ),
 ( #100178, #78355 ),
 ( #84483, #69764 ),
 ( #77353, #61171 ),
 ( #54051, #38802 ),
 ( #62664, #244 ),
 ( #31187, #39805 ),
 ( #39304, #30694 ),
 ( #70763, #14964 ),
 ( #63160, #32188 ),
 ( #62161, #84977 ),
 ( #93083, #31696 ),
 ( #54537, #45936 ),
 ( #92583, #94088 ),
 ( #23063, #37813 ),
 ( #68765, #76846 ),
 ( #15462, #46422 ),
 ( #24572, #70260 ),
 ( #23568, #85473 ),
 ( #16457, #55549 ),
 ( #15958, #46924 ),
 ( #99685, #7348 ),
 ( #30189, #8355 ),
 ( #93579, #55044 ),
 ( #85982, #34208 ),
 ( #3761, #2761 ),
 ( #26082, #10864 ),
 ( #79862, #11361 ),
 ( #79362, #34702 ),
 ( #95097, #10356 ),
 ( #65673, #72773 ),
 ( #41827, #88491 ),
 ( #41313, #96589 ),
 ( #72272, #33701 ),
 ( #25072, #40805 ),
 ( #27088, #49439 ),
 ( #64679, #42334 ),
 ( #57552, #94591 ),
 ( #48933, #49944 ),
 ( #26592, #17974 ),
 ( #56050, #80874 ),
 ( #18967, #65177 ),
 ( #95595, #58054 ),
 ( #73268, #16965 ),
 ( #57054, #80373 ),
 ( #47929, #87990 ),
 ( #25581, #2260 ),
 ( #9854, #18467 ),
 ( #32690, #3267 ),
 ( #78852, #71768 ),
 ( #86976, #9350 ),
 ( #33193, #96104 ),
 ( #40313, #71262 ),
 ( #1753, #63671 ),
 ( #17468, #64175 ),
 ( #48431, #56555 ),
 ( #87482, #13836 ),
 ( #29070, #66174 ),
 ( #44811, #42823 ),
 ( #19460, #74743 ),
 ( #5240, #43318 ),
 ( #75731, #21441 ),
 ( #82854, #51426 ),
 ( #12840, #97093 ),
 ( #98070, #51924 ),
 ( #99068, #28578 ),
 ( #97586, #74255 ),
 ( #50931, #20453 ),
 ( #4253, #82361 ),
 ( #29567, #81868 ),
 ( #58542, #81370 ),
 ( #4749, #59538 ),
 ( #43809, #20952 ),
 ( #67657, #90477 ),
 ( #50428, #12347 ),
 ( #36198, #35700 ),
 ( #66676, #88990 ),
 ( #28088, #59041 ),
 ( #13337, #98575 ),
 ( #6232, #44317 ),
 ( #35203, #89482 ),
 ( #75244, #36690 ),
 ( #5735, #83353 ),
 ( #67162, #11854 ),
 ( #60043, #37187 ),
 ( #90972, #73754 ),
 ( #52421, #68143 ),
 ( #27591, #19959 ),
 ( #89980, #22929 ),
 ( #76230, #22437 ),
 ( #47304, #38169 ),
 ( #100052, #78228 ),
 ( #31058, #54412 ),
 ( #8236, #92455 ),
 ( #6729, #53918 ),
 ( #1128, #53420 ),
 ( #30061, #52922 ),
 ( #76720, #62030 ),
 ( #85861, #15331 ),
 ( #70632, #54917 ),
 ( #68641, #69640 ),
 ( #84349, #61538 ),
 ( #7221, #60544 ),
 ( #14832, #69129 ),
 ( #92955, #39177 ),
 ( #16337, #23430 ),
 ( #37681, #61035 ),
 ( #15833, #70131 ),
 ( #62527, #85347 ),
 ( #46803, #31565 ),
 ( #84852, #99559 ),
 ( #30566, #46293 ),
 ( #77222, #8739 ),
 ( #93456, #118 ),
 ( #45799, #7729 ),
 ( #91966, #38676 ),
 ( #39678, #77723 ),
 ( #620, #91460 ),
 ( #23949, #21937 ),
 ( #83855, #14332 ),
 ( #45310, #71644 ),
 ( #94968, #17347 ),
 ( #88366, #79741 ),
 ( #93962, #24454 ),
 ( #32567, #10235 ),
 ( #18844, #95975 ),
 ( #3145, #41707 ),
 ( #42215, #71143 ),
 ( #63549, #72649 ),
 ( #48307, #2638 ),
 ( #25457, #80757 ),
 ( #9225, #16844 ),
 ( #34086, #40691 ),
 ( #79238, #32066 ),
 ( #65057, #1635 ),
 ( #56434, #40189 ),
 ( #41197, #95475 ),
 ( #73148, #72151 ),
 ( #2144, #9736 ),
 ( #94470, #64056 ),
 ( #24953, #26473 ),
 ( #55422, #57436 ),
 ( #86360, #49825 ),
 ( #33578, #47803 ),
 ( #87356, #64556 ),
 ( #10743, #25960 ),
 ( #33078, #11239 ),
 ( #17854, #56932 ),
 ( #63041, #78722 ),
 ( #48816, #55928 ),
 ( #86849, #87866 ),
 ( #18351, #49319 ),
 ( #80251, #65556 ),
 ( #66560, #58430 ),
 ( #98455, #11729 ),
 ( #13723, #50311 ),
 ( #59929, #88874 ),
 ( #21328, #67045 ),
 ( #96973, #36074 ),
 ( #34585, #89362 ),
 ( #82242, #52305 ),
 ( #27963, #57934 ),
 ( #81749, #97471 ),
 ( #90857, #59413 ),
 ( #83240, #28956 ),
 ( #27473, #58918 ),
 ( #43199, #89861 ),
 ( #50809, #44694 ),
 ( #51302, #3638 ),
 ( #96471, #36565 ),
 ( #12721, #20832 ),
 ( #67535, #26960 ),
 ( #13221, #4632 ),
 ( #42706, #19345 ),
 ( #44194, #51809 ),
 ( #74628, #97953 ),
 ( #81246, #20330 ),
 ( #28450, #73640 ),
 ( #43690, #4132 ),
 ( #90359, #35081 ),
 ( #66053, #19831 ),
 ( #5122, #12222 ),
 ( #74140, #35586 ),
 ( #82739, #75129 ),
 ( #5621, #29448 ),
 ( #30459, #12 ),
 ( #506, #85748 ),
 ( #46187, #69529 ),
 ( #23328, #37573 ),
 ( #85239, #77115 ),
 ( #15728, #22326 ),
 ( #31458, #22822 ),
 ( #53304, #92350 ),
 ( #46697, #77617 ),
 ( #39068, #62422 ),
 ( #30954, #6119 ),
 ( #93346, #53807 ),
 ( #83738, #23837 ),
 ( #76121, #7117 ),
 ( #54810, #70019 ),
 ( #7622, #91353 ),
 ( #8129, #84237 ),
 ( #16232, #14723 ),
 ( #6620, #68525 ),
 ( #38572, #21828 ),
 ( #38065, #75613 ),
 ( #37070, #45194 ),
 ( #68035, #91852 ),
 ( #98960, #84741 ),
 ( #61920, #60429 ),
 ( #52805, #14218 ),
 ( #99455, #29955 ),
 ( #60923, #45689 ),
 ( #76613, #69022 ),
 ( #99946, #92849 ),
 ( #61423, #15229 ),
 ( #54313, #93854 ),
 ( #8627, #2527 ),
 ( #57327, #41591 ),
 ( #10629, #32462 ),
 ( #9121, #48199 ),
 ( #39574, #88257 ),
 ( #79130, #33964 ),
 ( #64946, #72535 ),
 ( #3029, #94356 ),
 ( #25346, #18240 ),
 ( #78114, #9624 ),
 ( #79630, #95860 ),
 ( #71536, #47196 ),
 ( #72041, #26353 ),
 ( #70526, #1015 ),
 ( #17233, #40079 ),
 ( #49209, #56324 ),
 ( #71033, #40586 ),
 ( #62934, #1522 ),
 ( #2030, #33457 ),
 ( #31961, #24348 ),
 ( #17740, #41087 ),
 ( #95362, #63437 ),
 ( #56824, #48709 ),
 ( #87755, #24843 ),
 ( #55314, #94856 ),
 ( #55817, #63947 ),
 ( #80138, #86248 ),
 ( #16728, #32970 ),
 ( #47695, #78614 ),
 ( #86745, #87245 ),
 ( #10123, #64447 ),
 ( #25847, #89754 ),
 ( #37833, #13113 ),
 ( #51195, #34471 ),
 ( #20725, #27355 ),
 ( #99704, #58316 ),
 ( #19233, #81139 ),
 ( #82137, #65445 ),
 ( #50695, #61192 ),
 ( #80640, #88762 ),
 ( #59307, #34968 ),
 ( #11125, #44077 ),
 ( #12622, #43581 ),
 ( #18731, #76378 ),
 ( #82628, #96364 ),
 ( #74521, #66932 ),
 ( #51695, #20225 ),
 ( #5013, #90251 ),
 ( #81642, #26853 ),
 ( #89254, #12114 ),
 ( #35962, #43087 ),
 ( #4525, #6879 ),
 ( #97850, #42596 ),
 ( #68788, #57822 ),
 ( #30209, #49709 ),
 ( #28344, #42094 ),
 ( #73041, #3526 ),
 ( #50197, #11617 ),
 ( #74031, #73531 ),
 ( #35474, #4022 ),
 ( #65942, #96864 ),
 ( #19721, #66442 ),
 ( #97367, #27848 ),
 ( #58805, #9372 ),
 ( #24593, #63182 ),
 ( #77871, #78871 ),
 ( #46443, #100197 ),
 ( #55567, #92604 ),
 ( #71285, #40332 ),
 ( #47950, #24094 ),
 ( #77374, #94106 ),
 ( #92112, #7875 ),
 ( #38823, #86500 ),
 ( #23586, #55064 ),
 ( #85495, #54556 ),
 ( #16984, #22580 ),
 ( #39322, #32207 ),
 ( #30717, #1773 ),
 ( #8377, #47447 ),
 ( #32711, #53577 ),
 ( #69786, #84502 ),
 ( #93105, #70285 ),
 ( #14985, #7370 ),
 ( #15977, #45956 ),
 ( #76868, #765 ),
 ( #38322, #23082 ),
 ( #69282, #54073 ),
 ( #61686, #84997 ),
 ( #15481, #86002 ),
 ( #263, #31208 ),
 ( #62181, #46948 ),
 ( #31717, #62683 ),
 ( #93600, #16476 ),
 ( #78375, #8880 ),
 ( #39824, #70782 ),
 ( #1279, #3780 ),
 ( #34226, #56068 ),
 ( #18489, #96121 ),
 ( #42354, #72790 ),
 ( #48453, #72290 ),
 ( #64701, #10882 ),
 ( #73774, #79383 ),
 ( #95617, #50445 ),
 ( #81392, #58075 ),
 ( #89008, #10375 ),
 ( #64194, #25093 ),
 ( #11378, #87506 ),
 ( #65198, #33721 ),
 ( #34718, #11873 ),
 ( #9875, #2782 ),
 ( #26104, #40826 ),
 ( #57074, #42844 ),
 ( #65693, #3290 ),
 ( #17992, #88009 ),
 ( #49460, #17489 ),
 ( #41335, #80393 ),
 ( #4274, #18984 ),
 ( #63693, #19482 ),
 ( #48953, #41848 ),
 ( #26610, #57573 ),
 ( #79882, #71788 ),
 ( #25604, #94613 ),
 ( #88509, #49963 ),
 ( #96608, #27105 ),
 ( #86997, #80892 ),
 ( #73286, #2284 ),
 ( #33214, #95115 ),
 ( #56574, #36217 ),
 ( #45332, #43338 ),
 ( #19982, #27612 ),
 ( #35223, #67677 ),
 ( #75753, #58561 ),
 ( #37211, #82872 ),
 ( #90991, #76253 ),
 ( #60565, #99089 ),
 ( #5259, #98093 ),
 ( #66194, #51445 ),
 ( #12366, #59064 ),
 ( #28106, #98597 ),
 ( #97115, #91483 ),
 ( #29588, #81889 ),
 ( #21961, #89501 ),
 ( #90001, #29090 ),
 ( #74277, #59561 ),
 ( #4768, #60064 ),
 ( #43829, #28600 ),
 ( #52441, #90496 ),
 ( #20972, #68163 ),
 ( #21462, #20475 ),
 ( #52944, #50951 ),
 ( #83874, #14354 ),
 ( #51943, #74763 ),
 ( #83372, #6254 ),
 ( #35722, #13861 ),
 ( #13359, #66695 ),
 ( #44335, #82382 ),
 ( #12861, #97606 ),
 ( #44832, #67181 ),
 ( #75264, #5757 ),
 ( #36712, #24475 ),
 ( #39698, #78249 ),
 ( #7750, #16864 ),
 ( #70658, #7243 ),
 ( #23969, #22952 ),
 ( #639, #69662 ),
 ( #63062, #39196 ),
 ( #92478, #8760 ),
 ( #99581, #32086 ),
 ( #62552, #47824 ),
 ( #93984, #1150 ),
 ( #55441, #69152 ),
 ( #54436, #30086 ),
 ( #22458, #62053 ),
 ( #86381, #6749 ),
 ( #37703, #31587 ),
 ( #68663, #53444 ),
 ( #61057, #93477 ),
 ( #30588, #91987 ),
 ( #14855, #31081 ),
 ( #84374, #54939 ),
 ( #45822, #76741 ),
 ( #70154, #77246 ),
 ( #92978, #38194 ),
 ( #85881, #61559 ),
 ( #100072, #53943 ),
 ( #84873, #23453 ),
 ( #16358, #15354 ),
 ( #46318, #77742 ),
 ( #38696, #47326 ),
 ( #85370, #139 ),
 ( #15855, #46826 ),
 ( #8258, #34605 ),
 ( #78747, #40209 ),
 ( #11258, #79258 ),
 ( #95995, #65576 ),
 ( #32590, #34106 ),
 ( #64577, #96491 ),
 ( #33096, #86874 ),
 ( #42236, #9755 ),
 ( #57954, #26983 ),
 ( #88892, #10764 ),
 ( #64075, #80776 ),
 ( #9248, #94990 ),
 ( #25478, #73168 ),
 ( #79762, #19365 ),
 ( #72170, #10257 ),
 ( #40710, #71164 ),
 ( #1654, #18866 ),
 ( #63569, #3659 ),
 ( #49339, #17872 ),
 ( #33597, #41218 ),
 ( #17369, #2164 ),
 ( #94489, #41728 ),
 ( #95495, #24973 ),
 ( #49843, #55947 ),
 ( #48330, #71665 ),
 ( #56453, #25981 ),
 ( #56952, #87378 ),
 ( #48836, #2661 ),
 ( #87886, #18371 ),
 ( #80270, #72667 ),
 ( #3165, #65078 ),
 ( #26493, #57456 ),
 ( #88386, #83259 ),
 ( #51323, #98976 ),
 ( #43711, #82265 ),
 ( #12239, #11750 ),
 ( #42728, #90875 ),
 ( #20853, #73659 ),
 ( #5142, #82759 ),
 ( #28973, #59437 ),
 ( #35105, #58939 ),
 ( #12740, #35606 ),
 ( #66577, #91370 ),
 ( #74159, #97490 ),
 ( #68051, #44710 ),
 ( #13241, #13739 ),
 ( #50829, #4153 ),
 ( #98475, #97972 ),
 ( #90378, #81769 ),
 ( #21347, #37088 ),
 ( #66074, #89880 ),
 ( #74647, #96993 ),
 ( #36095, #29465 ),
 ( #52324, #51829 ),
 ( #28472, #60449 ),
 ( #67064, #27492 ),
 ( #44215, #75148 ),
 ( #75634, #50330 ),
 ( #6136, #5638 ),
 ( #27984, #36584 ),
 ( #81267, #58449 ),
 ( #89382, #67556 ),
 ( #19853, #59948 ),
 ( #43221, #4652 ),
 ( #20350, #78130 ),
 ( #22341, #53827 ),
 ( #39590, #16252 ),
 ( #68541, #30475 ),
 ( #23855, #61441 ),
 ( #7133, #21845 ),
 ( #54830, #60939 ),
 ( #70542, #31980 ),
 ( #93364, #6635 ),
 ( #83755, #91870 ),
 ( #62437, #14236 ),
 ( #85765, #69548 ),
 ( #77636, #62948 ),
 ( #47211, #8645 ),
 ( #1030, #84255 ),
 ( #28, #45211 ),
 ( #37591, #77134 ),
 ( #52820, #76138 ),
 ( #99473, #15748 ),
 ( #69037, #99965 ),
 ( #29970, #8147 ),
 ( #30971, #53325 ),
 ( #14740, #46202 ),
 ( #45706, #46713 ),
 ( #76632, #38083 ),
 ( #85255, #92368 ),
 ( #54330, #84758 ),
 ( #22839, #15246 ),
 ( #7642, #61938 ),
 ( #38588, #92868 ),
 ( #23345, #39084 ),
 ( #70038, #526 ),
 ( #31477, #25866 ),
 ( #64464, #32988 ),
 ( #48726, #56341 ),
 ( #1538, #17249 ),
 ( #63963, #86760 ),
 ( #25361, #24364 ),
 ( #47714, #72059 ),
 ( #2541, #17756 ),
 ( #80655, #71553 ),
 ( #94871, #11140 ),
 ( #64964, #42110 ),
 ( #56840, #87261 ),
 ( #79644, #10645 ),
 ( #10141, #79146 ),
 ( #48217, #55834 ),
 ( #87772, #40602 ),
 ( #18744, #33981 ),
 ( #71049, #73056 ),
 ( #95875, #3043 ),
 ( #3541, #32479 ),
 ( #94373, #26369 ),
 ( #9642, #95378 ),
 ( #41104, #34483 ),
 ( #18254, #33473 ),
 ( #49227, #80156 ),
 ( #41607, #93873 ),
 ( #2046, #24859 ),
 ( #72551, #57342 ),
 ( #88274, #78629 ),
 ( #49723, #55331 ),
 ( #86264, #16744 ),
 ( #9136, #40095 ),
 ( #63453, #21235 ),
 ( #74535, #4038 ),
 ( #74043, #35487 ),
 ( #50707, #65459 ),
 ( #6019, #42609 ),
 ( #81657, #58329 ),
 ( #59827, #59319 ),
 ( #12128, #43100 ),
 ( #36470, #90760 ),
 ( #51706, #96377 ),
 ( #20239, #73545 ),
 ( #75519, #11631 ),
 ( #52206, #50211 ),
 ( #4541, #34980 ),
 ( #27369, #44592 ),
 ( #66459, #82148 ),
 ( #43595, #82642 ),
 ( #28865, #83134 ),
 ( #20738, #26867 ),
 ( #13621, #12634 ),
 ( #65956, #57834 ),
 ( #96878, #97378 ),
 ( #88777, #19244 ),
 ( #89266, #27862 ),
 ( #67435, #58818 ),
 ( #89767, #81153 ),
 ( #19734, #51207 ),
 ( #5026, #35974 ),
 ( #66944, #97861 ),
 ( #28357, #90262 ),
 ( #5518, #13124 ),
 ( #98360, #44092 ),
 ( #75020, #47100 ),
 ( #62326, #410 ),
 ( #8021, #99362 ),
 ( #84642, #29356 ),
 ( #14123, #60829 ),
 ( #29857, #69426 ),
 ( #78016, #93255 ),
 ( #31362, #83641 ),
 ( #23741, #67939 ),
 ( #36974, #38971 ),
 ( #45101, #61329 ),
 ( #76022, #61826 ),
 ( #21730, #85651 ),
 ( #100344, #7022 ),
 ( #22725, #69924 ),
 ( #30860, #91748 ),
 ( #54715, #52703 ),
 ( #16131, #98863 ),
 ( #99848, #76516 ),
 ( #92748, #60332 ),
 ( #91256, #23232 ),
 ( #7520, #37972 ),
 ( #15630, #6526 ),
 ( #22228, #53211 ),
 ( #37477, #68427 ),
 ( #84139, #14629 ),
 ( #15132, #45596 ),
 ( #68923, #54218 ),
 ( #30355, #92253 ),
 ( #53715, #46095 ),
 ( #85143, #77020 ),
 ( #38475, #46597 ),
 ( #77522, #1426 ),
 ( #40484, #39479 ),
 ( #32362, #71437 ),
 ( #32873, #62838 ),
 ( #63845, #33359 ),
 ( #33868, #18631 ),
 ( #79537, #2426 ),
 ( #93756, #63339 ),
 ( #10025, #40987 ),
 ( #49110, #55722 ),
 ( #64853, #56222 ),
 ( #70431, #917 ),
 ( #80040, #10526 ),
 ( #26257, #1928 ),
 ( #41487, #18140 ),
 ( #49610, #47602 ),
 ( #9027, #72441 ),
 ( #39974, #94758 ),
 ( #57230, #2934 ),
 ( #55221, #17136 ),
 ( #95763, #48103 ),
 ( #94257, #8528 ),
 ( #70938, #24741 ),
 ( #71945, #24248 ),
 ( #25248, #31869 ),
 ( #86149, #78519 ),
 ( #88161, #86649 ),
 ( #16630, #79028 ),
 ( #64347, #9526 ),
 ( #17640, #87151 ),
 ( #48612, #95266 ),
 ( #25755, #56724 ),
 ( #87659, #42501 ),
 ( #27754, #72939 ),
 ( #96269, #35377 ),
 ( #67322, #43977 ),
 ( #74908, #74427 ),
 ( #27262, #58216 ),
 ( #51595, #5413 ),
 ( #66837, #80538 ),
 ( #66340, #88662 ),
 ( #90644, #26754 ),
 ( #19631, #89157 ),
 ( #65352, #97759 ),
 ( #12520, #12023 ),
 ( #34870, #34371 ),
 ( #28751, #89654 ),
 ( #57720, #36366 ),
 ( #4921, #35865 ),
 ( #21121, #19131 ),
 ( #28250, #82530 ),
 ( #3933, #43487 ),
 ( #97263, #42992 ),
 ( #50103, #65843 ),
 ( #59714, #59210 ),
 ( #58704, #98247 ),
 ( #20628, #81043 ),
 ( #73931, #13011 ),
 ( #11032, #20134 ),
 ( #51096, #96763 ),
 ( #42001, #3438 ),
 ( #4426, #11522 ),
 ( #82041, #90153 ),
 ( #73437, #50594 ),
 ( #81550, #92136 ),
 ( #60714, #37370 ),
 ( #14009, #84026 ),
 ( #67828, #45487 ),
 ( #93131, #44985 ),
 ( #21617, #44481 ),
 ( #68313, #22608 ),
 ( #77401, #6905 ),
 ( #30743, #61217 ),
 ( #36864, #84525 ),
 ( #76402, #14512 ),
 ( #75909, #13510 ),
 ( #75406, #92633 ),
 ( #53602, #5907 ),
 ( #37858, #15012 ),
 ( #61710, #45980 ),
 ( #98751, #91633 ),
 ( #68812, #99245 ),
 ( #62209, #29242 ),
 ( #99732, #38853 ),
 ( #69810, #46471 ),
 ( #76894, #15504 ),
 ( #52586, #60212 ),
 ( #100226, #30235 ),
 ( #7396, #83523 ),
 ( #23111, #291 ),
 ( #91141, #22117 ),
 ( #38354, #6414 ),
 ( #29747, #69306 ),
 ( #83021, #53099 ),
 ( #54100, #31240 ),
 ( #85020, #7901 ),
 ( #52092, #48486 ),
 ( #50348, #35121 ),
 ( #94642, #17520 ),
 ( #55599, #25120 ),
 ( #40855, #78904 ),
 ( #8906, #31745 ),
 ( #71316, #23613 ),
 ( #16008, #57971 ),
 ( #1804, #71821 ),
 ( #88910, #81287 ),
 ( #79412, #54587 ),
 ( #11770, #40362 ),
 ( #62714, #42744 ),
 ( #24124, #86528 ),
 ( #73677, #19381 ),
 ( #70314, #32237 ),
 ( #63212, #85523 ),
 ( #46976, #39852 ),
 ( #93628, #24618 ),
 ( #4170, #9401 ),
 ( #9903, #66094 ),
 ( #77899, #56097 ),
 ( #96508, #8403 ),
 ( #87029, #3676 ),
 ( #34624, #65593 ),
 ( #39355, #793 ),
 ( #27004, #70815 ),
 ( #55095, #86028 ),
 ( #16505, #47476 ),
 ( #78405, #1304 ),
 ( #32741, #94135 ),
 ( #17014, #47978 ),
 ( #63724, #74176 ),
 ( #21366, #59963 ),
 ( #74664, #50848 ),
 ( #13259, #5654 ),
 ( #97991, #52340 ),
 ( #97507, #4671 ),
 ( #82283, #59453 ),
 ( #12758, #51342 ),
 ( #35621, #27511 ),
 ( #58466, #75164 ),
 ( #28491, #89401 ),
 ( #5161, #90398 ),
 ( #98490, #28991 ),
 ( #28002, #36604 ),
 ( #58959, #97009 ),
 ( #19873, #66595 ),
 ( #43730, #20367 ),
 ( #90891, #81787 ),
 ( #67573, #12259 ),
 ( #36112, #89899 ),
 ( #43238, #67081 ),
 ( #20872, #51843 ),
 ( #82777, #44233 ),
 ( #45666, #24318 ),
 ( #76591, #78090 ),
 ( #93324, #92823 ),
 ( #15205, #14701 ),
 ( #9096, #69994 ),
 ( #78586, #55291 ),
 ( #86221, #7594 ),
 ( #39046, #31939 ),
 ( #91827, #47171 ),
 ( #62909, #15706 ),
 ( #85218, #71008 ),
 ( #46670, #40051 ),
 ( #77095, #7095 ),
 ( #54290, #47672 ),
 ( #93832, #480 ),
 ( #84714, #23305 ),
 ( #77593, #38044 ),
 ( #8097, #85722 ),
 ( #16704, #1498 ),
 ( #31434, #54787 ),
 ( #68997, #46165 ),
 ( #8603, #62393 ),
 ( #38546, #99921 ),
 ( #22798, #60901 ),
 ( #69502, #23814 ),
 ( #990, #22304 ),
 ( #53282, #16204 ),
 ( #84210, #70501 ),
 ( #30432, #61402 ),
 ( #92325, #53784 ),
 ( #100419, #39549 ),
 ( #30930, #61898 ),
 ( #95334, #73009 ),
 ( #72508, #42563 ),
 ( #11586, #41054 ),
 ( #32941, #94829 ),
 ( #64916, #48171 ),
 ( #64417, #73495 ),
 ( #94327, #1995 ),
 ( #3496, #48681 ),
 ( #24812, #57784 ),
 ( #88230, #32435 ),
 ( #88728, #96331 ),
 ( #2494, #25822 ),
 ( #63409, #79605 ),
 ( #9598, #56295 ),
 ( #25319, #95829 ),
 ( #17206, #26819 ),
 ( #50168, #26324 ),
 ( #87217, #57298 ),
 ( #55793, #17711 ),
 ( #56794, #19197 ),
 ( #10095, #81105 ),
 ( #72013, #87728 ),
 ( #86716, #18694 ),
 ( #79099, #40558 ),
 ( #18210, #3001 ),
 ( #33937, #11095 ),
 ( #33432, #71511 ),
 ( #80106, #63915 ),
 ( #49182, #65416 ),
 ( #34437, #10593 ),
 ( #41560, #49676 ),
 ( #42064, #80603 ),
 ( #43053, #36923 ),
 ( #44544, #21189 ),
 ( #74973, #98312 ),
 ( #52652, #28313 ),
 ( #66898, #75469 ),
 ( #44042, #14075 ),
 ( #83588, #12587 ),
 ( #66409, #35927 ),
 ( #19690, #97820 ),
 ( #45052, #97329 ),
 ( #74000, #96826 ),
 ( #20192, #5476 ),
 ( #29309, #59269 ),
 ( #60282, #83084 ),
 ( #4493, #89222 ),
 ( #74487, #90217 ),
 ( #3990, #51157 ),
 ( #20691, #51662 ),
 ( #67892, #21680 ),
 ( #28815, #98815 ),
 ( #50661, #35440 ),
 ( #59781, #52155 ),
 ( #27322, #36424 ),
 ( #67388, #5973 ),
 ( #91205, #82106 ),
 ( #58283, #34933 ),
 ( #90715, #65911 ),
 ( #81609, #12080 ),
 ( #27817, #58770 ),
 ( #82599, #89722 ),
 ( #43550, #13075 ),
 ( #4980, #13575 ),
 ( #70376, #69875 ),
 ( #22678, #53664 ),
 ( #37431, #31306 ),
 ( #23182, #99314 ),
 ( #76470, #77468 ),
 ( #22181, #85590 ),
 ( #39426, #38422 ),
 ( #38921, #46049 ),
 ( #7968, #7463 ),
 ( #30303, #29807 ),
 ( #24192, #85091 ),
 ( #60778, #865 ),
 ( #358, #62275 ),
 ( #86096, #91697 ),
 ( #93200, #47048 ),
 ( #23686, #54660 ),
 ( #16077, #77962 ),
 ( #55169, #31818 ),
 ( #75971, #68381 ),
 ( #8476, #6975 ),
 ( #62787, #93701 ),
 ( #16574, #53164 ),
 ( #6479, #61776 ),
 ( #92695, #61280 ),
 ( #84093, #14579 ),
 ( #45549, #69373 ),
 ( #100293, #37924 ),
 ( #68872, #30811 ),
 ( #99796, #15576 ),
 ( #92203, #84593 ),
 ( #76968, #15082 ),
 ( #54169, #46540 ),
 ( #39924, #49553 ),
 ( #79982, #95215 ),
 ( #41429, #18578 ),
 ( #18088, #87096 ),
 ( #2373, #9973 ),
 ( #55669, #71386 ),
 ( #26704, #10471 ),
 ( #64292, #72885 ),
 ( #88110, #24686 ),
 ( #79486, #80482 ),
 ( #57174, #48559 ),
 ( #25696, #1869 ),
 ( #3384, #10978 ),
 ( #72388, #40927 ),
 ( #71889, #49054 ),
 ( #41943, #33304 ),
 ( #57663, #87606 ),
 ( #56168, #32815 ),
 ( #9473, #56671 ),
 ( #63284, #2883 ),
 ( #88606, #40433 ),
 ( #17082, #70887 ),
 ( #63792, #33813 ),
 ( #64797, #95714 ),
 ( #26202, #34319 ),
 ( #32310, #17587 ),
 ( #65296, #94708 ),
 ( #25191, #47549 ),
 ( #96220, #78471 ),
 ( #8971, #1377 ),
 ( #94201, #86596 ),
 ( #48046, #78976 ),
 ( #74856, #67274 ),
 ( #21071, #74368 ),
 ( #43438, #29194 ),
 ( #28702, #3880 ),
 ( #81986, #36812 ),
 ( #89599, #11972 ),
 ( #52039, #28199 ),
 ( #42940, #12469 ),
 ( #34818, #81492 ),
 ( #5856, #97208 ),
 ( #58651, #67780 ),
 ( #98698, #4864 ),
 ( #35813, #59662 ),
 ( #59156, #60165 ),
 ( #19078, #27705 ),
 ( #19578, #73874 ),
 ( #51545, #65789 ),
 ( #51047, #50051 ),
 ( #80989, #89104 ),
 ( #90592, #35322 ),
 ( #82968, #66787 ),
 ( #75356, #98192 ),
 ( #58161, #96704 ),
 ( #20079, #97705 ),
 ( #11472, #66283 ),
 ( #27207, #4374 ),
 ( #90100, #82477 ),
 ( #42446, #73385 ),
 ( #13458, #50538 ),
 ( #20574, #5360 ),
 ( #12957, #43926 ),
 ( #36314, #44432 ),
 ( #37315, #237 ),
 ( #91583, #6850 ),
 ( #7846, #84474 ),
 ( #76838, #93076 ),
 ( #84968, #14454 ),
 ( #85465, #6359 ),
 ( #8347, #77840 ),
 ( #53543, #30180 ),
 ( #46414, #62153 ),
 ( #23560, #75855 ),
 ( #23053, #92575 ),
 ( #69755, #31179 ),
 ( #70252, #46916 ),
 ( #91087, #52535 ),
 ( #54530, #22063 ),
 ( #68262, #39295 ),
 ( #15950, #735 ),
 ( #92082, #31688 ),
 ( #21563, #53044 ),
 ( #83471, #83974 ),
 ( #13958, #44934 ),
 ( #30685, #99190 ),
 ( #29691, #99677 ),
 ( #45433, #76349 ),
 ( #54043, #60661 ),
 ( #22552, #37805 ),
 ( #68757, #61163 ),
 ( #14954, #45927 ),
 ( #7340, #38295 ),
 ( #69251, #100169 ),
 ( #61656, #15454 ),
 ( #77346, #38795 ),
 ( #62655, #78843 ),
 ( #39796, #86472 ),
 ( #55541, #96463 ),
 ( #4624, #19822 ),
 ( #27463, #8848 ),
 ( #24066, #19333 ),
 ( #11229, #85973 ),
 ( #70754, #88357 ),
 ( #1251, #73632 ),
 ( #58421, #26464 ),
 ( #81239, #57427 ),
 ( #49815, #66046 ),
 ( #57925, #16958 ),
 ( #89355, #78347 ),
 ( #81739, #50800 ),
 ( #18833, #1744 ),
 ( #50303, #35073 ),
 ( #96963, #47419 ),
 ( #26952, #65546 ),
 ( #42698, #4123 ),
 ( #43190, #12214 ),
 ( #93571, #55036 ),
 ( #74131, #63153 ),
 ( #11718, #16449 ),
 ( #32180, #94079 ),
 ( #63662, #24564 ),
 ( #47922, #9343 ),
 ( #40306, #71255 ),
 ( #32683, #94584 ),
 ( #80745, #42206 ),
 ( #3629, #73138 ),
 ( #34578, #88866 ),
 ( #67522, #68023 ),
 ( #28947, #98445 ),
 ( #97943, #97461 ),
 ( #27952, #76108 ),
 ( #6107, #58908 ),
 ( #98950, #91839 ),
 ( #44684, #74617 ),
 ( #44182, #5610 ),
 ( #20822, #35573 ),
 ( #76603, #12712 ),
 ( #51797, #28438 ),
 ( #14209, #66551 ),
 ( #29439, #99446 ),
 ( #36060, #89849 ),
 ( #83728, #83230 ),
 ( #90848, #43678 ),
 ( #45680, #82232 ),
 ( #20319, #29942 ),
 ( #53294, #60418 ),
 ( #22316, #21319 ),
 ( #75602, #91342 ),
 ( #59916, #60913 ),
 ( #59402, #84224 ),
 ( #13210, #52292 ),
 ( #14713, #21817 ),
 ( #52792, #6610 ),
 ( #90350, #45184 ),
 ( #37058, #37562 ),
 ( #82729, #51291 ),
 ( #13710, #5111 ),
 ( #67036, #68513 ),
 ( #75115, #36554 ),
 ( #71023, #63425 ),
 ( #16718, #8114 ),
 ( #46177, #40069 ),
 ( #94343, #1513 ),
 ( #39058, #86733 ),
 ( #32451, #93335 ),
 ( #15717, #55305 ),
 ( #46685, #24830 ),
 ( #55807, #1005 ),
 ( #54302, #85230 ),
 ( #78601, #17221 ),
 ( #93845, #7108 ),
 ( #62410, #15220 ),
 ( #48187, #70009 ),
 ( #38055, #494 ),
 ( #70514, #77607 ),
 ( #39564, #31447 ),
 ( #61910, #61413 ),
 ( #69009, #16219 ),
 ( #92338, #99935 ),
 ( #31951, #62923 ),
 ( #30447, #22812 ),
 ( #24335, #9110 ),
 ( #78103, #23827 ),
 ( #54800, #85736 ),
 ( #77106, #30944 ),
 ( #53797, #86236 ),
 ( #47184, #84729 ),
 ( #47686, #7608 ),
 ( #38562, #69516 ),
 ( #15063, #8616 ),
 ( #92836, #23319 ),
 ( #34953, #11605 ),
 ( #73027, #41577 ),
 ( #3018, #80624 ),
 ( #19217, #33954 ),
 ( #89240, #18715 ),
 ( #87744, #64435 ),
 ( #41071, #10616 ),
 ( #94844, #72525 ),
 ( #19709, #72029 ),
 ( #48697, #71526 ),
 ( #2015, #17730 ),
 ( #64933, #11112 ),
 ( #57804, #88246 ),
 ( #63934, #18229 ),
 ( #95850, #95351 ),
 ( #25836, #79119 ),
 ( #2512, #56812 ),
 ( #25335, #42582 ),
 ( #96848, #42082 ),
 ( #33446, #3513 ),
 ( #9613, #49198 ),
 ( #26342, #73519 ),
 ( #80124, #27343 ),
 ( #34458, #65433 ),
 ( #40574, #32958 ),
 ( #96352, #50185 ),
 ( #57315, #26840 ),
 ( #88750, #81124 ),
 ( #49695, #58302 ),
 ( #4009, #56313 ),
 ( #87232, #65928 ),
 ( #79620, #10112 ),
 ( #82616, #83612 ),
 ( #60302, #51683 ),
 ( #89742, #14097 ),
 ( #91226, #67915 ),
 ( #21210, #44565 ),
 ( #45073, #36445 ),
 ( #59290, #98835 ),
 ( #90236, #50682 ),
 ( #81628, #66918 ),
 ( #12607, #13095 ),
 ( #66429, #44063 ),
 ( #91721, #43569 ),
 ( #20210, #43072 ),
 ( #97838, #52176 ),
 ( #75993, #5496 ),
 ( #6501, #29331 ),
 ( #51180, #35459 ),
 ( #20710, #74995 ),
 ( #12102, #28332 ),
 ( #74505, #67411 ),
 ( #83108, #21703 ),
 ( #37451, #13597 ),
 ( #97350, #82123 ),
 ( #5994, #52675 ),
 ( #74017, #90737 ),
 ( #75492, #68402 ),
 ( #98331, #27836 ),
 ( #4512, #36944 ),
 ( #28838, #58791 ),
 ( #5000, #59803 ),
 ( #35948, #99334 ),
 ( #29830, #60801 ),
 ( #39450, #15599 ),
 ( #7992, #24216 ),
 ( #16102, #46070 ),
 ( #16596, #37943 ),
 ( #39947, #8993 ),
 ( #85114, #61798 ),
 ( #77986, #93723 ),
 ( #55191, #6996 ),
 ( #54682, #23711 ),
 ( #887, #62809 ),
 ( #1398, #78493 ),
 ( #22201, #84116 ),
 ( #86119, #22698 ),
 ( #70399, #70907 ),
 ( #47573, #32333 ),
 ( #23205, #63306 ),
 ( #53185, #53685 ),
 ( #14600, #84616 ),
 ( #45572, #76489 ),
 ( #38941, #68892 ),
 ( #31840, #99819 ),
 ( #30325, #7488 ),
 ( #38444, #61300 ),
 ( #54190, #92226 ),
 ( #15104, #76990 ),
 ( #69396, #100316 ),
 ( #85613, #69896 ),
 ( #30833, #92717 ),
 ( #381, #8500 ),
 ( #46562, #77491 ),
 ( #31329, #62298 ),
 ( #93222, #47071 ),
 ( #3902, #9495 ),
 ( #25720, #81013 ),
 ( #11492, #88631 ),
 ( #19100, #40951 ),
 ( #50073, #26225 ),
 ( #72412, #65321 ),
 ( #24711, #80508 ),
 ( #96242, #49079 ),
 ( #18113, #34841 ),
 ( #80006, #73408 ),
 ( #9995, #78998 ),
 ( #87629, #42469 ),
 ( #26726, #2905 ),
 ( #17611, #56698 ),
 ( #40457, #56193 ),
 ( #10494, #18600 ),
 ( #94225, #55691 ),
 ( #64823, #88132 ),
 ( #71406, #48583 ),
 ( #95736, #57199 ),
 ( #34343, #71913 ),
 ( #86619, #41454 ),
 ( #17105, #48070 ),
 ( #57686, #1893 ),
 ( #32839, #33835 ),
 ( #49576, #63814 ),
 ( #94728, #11000 ),
 ( #25215, #87117 ),
 ( #79507, #41967 ),
 ( #2396, #33326 ),
 ( #64317, #95236 ),
 ( #72910, #3407 ) ),
 .UNSPECIFIED., .F., .F., .F.,
 ( 4, 2, 2, 2, 2, 2, 2, 2, 2, 2, 2, 2, 2, 2, 2, 2, 2, 2, 2, 2, 2, 2, 2, 2, 2, 2, 2, 2, 2, 2, 2, 2, 2, 2, 2, 2, 2, 2, 2, 2, 2, 2, 2, 2, 2, 2, 2, 2, 2, 2, 2, 2, 2, 2, 2, 2, 2, 2, 2, 2, 2, 2, 2, 2, 2, 2, 2, 2, 2, 2, 2, 2, 2, 2, 2, 2, 2, 2, 2, 2, 2, 2, 2, 2, 2, 2, 2, 2, 2, 2, 2, 2, 2, 2, 2, 2, 2, 2, 2, 2, 2, 2, 2, 2, 2, 2, 2, 2, 2, 2, 2, 2, 2, 2, 2, 2, 2, 2, 2, 2, 2, 2, 2, 2, 2, 2, 2, 2, 2, 2, 2, 2, 2, 2, 2, 2, 2, 2, 2, 2, 2, 2, 2, 2, 2, 2, 2, 2, 2, 2, 2, 2, 2, 2, 2, 2, 2, 2, 2, 2, 2, 2, 2, 2, 2, 2, 2, 2, 2, 2, 2, 2, 2, 2, 2, 2, 2, 2, 2, 2, 2, 2, 2, 2, 2, 2, 2, 2, 2, 2, 2, 2, 2, 2, 2, 2, 2, 2, 2, 2, 2, 2, 2, 2, 2, 2, 2, 2, 2, 2, 2, 2, 2, 2, 2, 2, 2, 2, 2, 2, 2, 2, 2, 2, 2, 2, 2, 2, 2, 2, 2, 2, 2, 2, 2, 2, 2, 2, 2, 2, 2, 2, 2, 2, 2, 2, 2, 2, 2, 2, 2, 2, 2, 2, 2, 2, 2, 2, 2, 2, 2, 2, 2, 2, 2, 2, 2, 2, 2, 2, 2, 2, 2, 2, 2, 2, 2, 2, 2, 2, 2, 2, 2, 2, 2, 2, 2, 2, 2, 2, 2, 2, 2, 2, 2, 2, 2, 2, 2, 2, 2, 2, 2, 2, 2, 2, 2, 2, 2, 2, 2, 2, 2, 2, 2, 2, 2, 2, 2, 2, 2, 2, 2, 2, 2, 2, 2, 2, 2, 2, 2, 2, 2, 2, 2, 2, 2, 2, 2, 2, 2, 2, 2, 2, 2, 2, 2, 2, 2, 2, 2, 2, 2, 2, 2, 2, 2, 2, 2, 2, 2, 2, 2, 2, 2, 2, 2, 2, 2, 2, 2, 2, 2, 2, 2, 2, 2, 2, 2, 2, 2, 2, 2, 2, 2, 2, 2, 2, 2, 2, 2, 2, 2, 2, 2, 2, 2, 2, 2, 2, 2, 2, 2, 2, 2, 2, 2, 2, 2, 2, 2, 2, 2, 2, 2, 2, 2, 2, 2, 2, 2, 2, 2, 2, 2, 2, 2, 2, 2, 2, 2, 2, 2, 2, 2, 2, 2, 2, 2, 2, 2, 2, 2, 2, 2, 2, 2, 2, 2, 2, 2, 2, 2, 2, 2, 2, 2, 2, 2, 2, 2, 2, 2, 2, 2, 2, 2, 2, 2, 2, 2, 2, 2, 2, 2, 2, 2, 2, 2, 2, 2, 2, 2, 2, 2, 2, 2, 2, 2, 2, 2, 2, 2, 2, 2, 2, 2, 2, 2, 2, 2, 2, 2, 2, 2, 2, 2, 2, 2, 2, 2, 2, 2, 2, 2, 2, 2, 2, 2, 2, 2, 2, 2, 2, 2, 2, 2, 2, 2, 2, 2, 2, 2, 2, 2, 2, 2, 2, 2, 2, 2, 2, 2, 2, 2, 2, 2, 2, 2, 2, 2, 2, 2, 2, 2, 2, 2, 2, 2, 2, 2, 2, 2, 2, 2, 2, 2, 2, 2, 2, 2, 2, 2, 2, 2, 2, 2, 2, 2, 2, 2, 2, 2, 2, 2, 2, 2, 2, 2, 2, 2, 2, 2, 2, 2, 2, 2, 2, 2, 2, 2, 2, 2, 2, 2, 2, 2, 2, 2, 2, 2, 2, 2, 2, 2, 2, 2, 2, 2, 2, 2, 2, 2, 2, 2, 2, 2, 2, 2, 2, 2, 2, 2, 2, 2, 2, 2, 2, 2, 2, 2, 2, 2, 2, 2, 2, 2, 2, 2, 2, 2, 2, 2, 2, 2, 2, 2, 2, 2, 2, 2, 2, 2, 2, 2, 2, 2, 2, 2, 2, 2, 2, 2, 2, 2, 2, 2, 2, 2, 2, 2, 2, 2, 2, 2, 2, 2, 2, 2, 2, 2, 2, 2, 2, 2, 2, 2, 2, 2, 2, 2, 2, 2, 2, 2, 2, 2, 2, 2, 2, 2, 2, 2, 2, 2, 2, 2, 2, 2, 2, 2, 2, 2, 2, 2, 2, 2, 2, 2, 2, 2, 2, 2, 2, 2, 2, 2, 2, 2, 2, 2, 2, 2, 2, 2, 2, 2, 2, 2, 2, 2, 2, 2, 2, 2, 2, 2, 2, 2, 2, 2, 2, 2, 2, 2, 2, 2, 2, 2, 2, 2, 2, 2, 2, 2, 2, 2, 2, 2, 2, 2, 2, 2, 2, 2, 2, 2, 2, 2, 2, 2, 2, 2, 2, 2, 2, 2, 2, 2, 2, 2, 2, 2, 2, 2, 2, 2, 2, 2, 2, 2, 2, 2, 2, 2, 2, 2, 2, 2, 2, 2, 2, 2, 2, 2, 2, 2, 2, 2, 2, 2, 2, 2, 2, 2, 2, 2, 2, 2, 2, 2, 2, 2, 2, 2, 2, 2, 2, 2, 2, 2, 2, 2, 2, 2, 2, 2, 2, 2, 2, 2, 2, 2, 2, 2, 2, 2, 2, 2, 2, 2, 2, 2, 2, 2, 2, 2, 2, 2, 2, 2, 2, 2, 2, 2, 2, 2, 2, 2, 2, 2, 2, 2, 2, 2, 2, 2, 2, 2, 2, 2, 2, 2, 2, 2, 2, 2, 2, 2, 2, 2, 2, 2, 2, 2, 2, 2, 2, 2, 2, 2, 2, 2, 2, 2, 2, 2, 2, 2, 2, 2, 2, 2, 2, 2, 2, 2, 2, 2, 2, 2, 2, 2, 2, 2, 2, 2, 2, 2, 2, 2, 2, 2, 2, 2, 2, 2, 2, 2, 2, 2, 2, 2, 2, 2, 2, 2, 2, 2, 2, 2, 2, 2, 2, 2, 2, 2, 2, 2, 2, 2, 2, 2, 2, 2, 2, 2, 2, 2, 2, 2, 2, 2, 2, 2, 2, 2, 2, 2, 2, 2, 2, 2, 2, 2, 2, 2, 2, 2, 2, 2, 2, 2, 2, 2, 2, 2, 2, 2, 2, 2, 2, 2, 2, 2, 2, 2, 2, 2, 2, 2, 2, 2, 2, 2, 2, 2, 2, 2, 2, 2, 2, 2, 2, 2, 2, 2, 2, 2, 2, 2, 2, 2, 2, 2, 2, 2, 2, 2, 2, 2, 2, 2, 2, 2, 2, 2, 2, 2, 2, 2, 2, 2, 2, 2, 2, 2, 2, 2, 2, 2, 2, 2, 2, 2, 2, 2, 2, 2, 2, 2, 2, 2, 2, 2, 2, 2, 2, 2, 2, 2, 2, 2, 2, 2, 2, 2, 2, 2, 2, 2, 2, 2, 2, 2, 2, 2, 2, 2, 2, 2, 2, 2, 2, 2, 2, 2, 2, 2, 2, 2, 2, 2, 2, 2, 2, 2, 2, 2, 2, 2, 2, 2, 2, 2, 2, 2, 2, 2, 2, 2, 2, 2, 2, 2, 2, 2, 2, 2, 2, 2, 2, 2, 2, 2, 2, 2, 2, 2, 2, 2, 2, 2, 2, 2, 2, 2, 2, 2, 2, 2, 2, 2, 2, 2, 2, 2, 2, 2, 2, 2, 2, 2, 2, 2, 2, 2, 2, 2, 2, 2, 2, 2, 2, 2, 2, 2, 2, 2, 2, 2, 2, 2, 2, 2, 2, 2, 2, 2, 2, 2, 2, 2, 2, 2, 2, 2, 2, 2, 2, 2, 2, 2, 2, 2, 2, 2, 2, 2, 2, 2, 2, 2, 2, 2, 2, 2, 2, 2, 2, 2, 2, 2, 2, 2, 2, 2, 2, 2, 2, 2, 2, 2, 2, 2, 2, 2, 2, 2, 2, 2, 2, 2, 2, 2, 2, 2, 2, 2, 2, 2, 2, 2, 2, 2, 2, 2, 2, 2, 2, 2, 2, 2, 2, 2, 2, 2, 2, 2, 2, 2, 2, 2, 2, 2, 2, 2, 2, 2, 2, 2, 2, 2, 2, 2, 2, 2, 2, 2, 2, 2, 2, 2, 2, 2, 2, 2, 2, 2, 2, 2, 2, 2, 2, 2, 2, 2, 2, 2, 2, 2, 2, 2, 2, 2, 2, 2, 2, 2, 2, 2, 2, 2, 2, 2, 2, 2, 2, 2, 2, 2, 2, 2, 2, 2, 2, 2, 2, 2, 2, 2, 2, 2, 2, 2, 2, 2, 2, 2, 2, 2, 2, 2, 2, 2, 2, 2, 2, 2, 2, 2, 2, 2, 2, 2, 2, 2, 2, 2, 2, 2, 2, 2, 2, 2, 2, 2, 2, 2, 2, 2, 2, 2, 2, 2, 2, 2, 2, 2, 2, 2, 2, 2, 2, 2, 2, 2, 2, 2, 2, 2, 2, 2, 2, 2, 2, 2, 2, 2, 2, 2, 2, 2, 2, 2, 2, 2, 2, 2, 2, 2, 2, 2, 2, 2, 2, 2, 2, 2, 2, 2, 2, 2, 2, 2, 2, 2, 2, 2, 2, 2, 2, 2, 2, 2, 2, 2, 2, 2, 2, 2, 2, 2, 2, 2, 2, 2, 2, 2, 2, 2, 2, 2, 2, 2, 2, 2, 2, 2, 2, 2, 2, 2, 2, 2, 2, 2, 2, 2, 2, 2, 2, 2, 2, 2, 2, 2, 2, 2, 2, 2, 2, 2, 2, 2, 2, 2, 2, 2, 2, 2, 2, 2, 2, 2, 2, 2, 2, 2, 2, 2, 2, 2, 2, 2, 2, 2, 2, 2, 2, 2, 2, 2, 2, 2, 2, 2, 2, 2, 2, 2, 2, 2, 2, 2, 2, 2, 2, 2, 2, 2, 2, 2, 2, 2, 2, 2, 2, 2, 2, 2, 2, 2, 2, 2, 2, 2, 2, 2, 2, 2, 2, 2, 2, 2, 2, 2, 2, 2, 2, 2, 2, 2, 2, 2, 2, 2, 2, 2, 2, 2, 2, 2, 2, 2, 2, 2, 2, 2, 2, 2, 2, 2, 2, 2, 2, 2, 2, 2, 2, 2, 2, 2, 2, 2, 2, 2, 2, 2, 2, 2, 2, 2, 2, 2, 2, 2, 2, 2, 2, 2, 2, 2, 2, 2, 2, 2, 2, 2, 2, 2, 2, 2, 2, 2, 2, 2, 2, 2, 2, 2, 2, 2, 2, 2, 2, 2, 2, 2, 2, 2, 2, 2, 2, 2, 2, 2, 2, 2, 2, 2, 2, 2, 2, 2, 2, 2, 2, 2, 2, 2, 2, 2, 2, 2, 2, 2, 2, 2, 2, 2, 2, 2, 2, 2, 2, 2, 2, 2, 2, 2, 2, 2, 2, 2, 2, 2, 2, 2, 2, 2, 2, 2, 2, 2, 2, 2, 2, 2, 2, 2, 2, 2, 2, 2, 2, 2, 2, 2, 2, 2, 2, 2, 2, 2, 2, 2, 2, 2, 2, 2, 2, 2, 2, 2, 2, 2, 2, 2, 2, 2, 2, 2, 2, 2, 2, 2, 2, 2, 2, 2, 2, 2, 2, 2, 2, 2, 2, 2, 2, 2, 2, 2, 2, 2, 2, 2, 2, 2, 2, 2, 2, 2, 2, 2, 2, 2, 2, 2, 2, 2, 2, 2, 2, 2, 2, 2, 2, 2, 2, 2, 2, 2, 2, 2, 2, 2, 2, 2, 2, 2, 2, 2, 2, 2, 2, 2, 2, 2, 2, 2, 2, 2, 2, 2, 2, 2, 2, 2, 2, 2, 2, 2, 2, 2, 2, 2, 2, 2, 2, 2, 2, 2, 2, 2, 2, 2, 2, 2, 2, 2, 2, 2, 2, 2, 2, 2, 2, 2, 2, 2, 2, 2, 2, 2, 2, 2, 2, 2, 2, 2, 2, 2, 2, 2, 2, 2, 2, 2, 2, 2, 2, 2, 2, 2, 2, 2, 2, 2, 2, 2, 2, 2, 2, 2, 2, 2, 2, 2, 2, 2, 2, 2, 2, 2, 2, 2, 2, 2, 2, 2, 2, 2, 2, 2, 2, 2, 2, 2, 2, 2, 2, 2, 2, 2, 2, 2, 2, 2, 2, 2, 2, 2, 2, 2, 2, 2, 2, 2, 2, 2, 2, 2, 2, 2, 2, 2, 2, 2, 2, 2, 2, 2, 2, 2, 2, 2, 2, 2, 2, 2, 2, 2, 2, 2, 2, 2, 2, 2, 2, 2, 2, 2, 2, 2, 2, 2, 2, 2, 2, 2, 2, 2, 2, 2, 2, 2, 2, 2, 2, 2, 2, 2, 2, 2, 2, 2, 2, 2, 2, 2, 2, 2, 2, 2, 2, 2, 2, 2, 2, 2, 2, 2, 2, 2, 2, 2, 2, 2, 2, 2, 2, 2, 2, 2, 2, 2, 2, 4 ),
 ( 2, 2 ),
 ( 0.000000000000000000, 0.0004882812500000001084, 0.0009765625000000002168, 0.001464843750000000434, 0.001953125000000000000, 0.002441406250000000000, 0.002929687499999999566, 0.003417968749999999566, 0.003906249999999999133, 0.004394531249999998265, 0.004882812499999997398, 0.005371093749999997398, 0.005859374999999997398, 0.006347656249999998265, 0.006835937499999998265, 0.007324218749999998265, 0.007812499999999998265, 0.008300781249999998265, 0.008789062499999998265, 0.009277343749999998265, 0.009765624999999998265, 0.01025390624999999827, 0.01074218749999999827, 0.01123046874999999827, 0.01171874999999999827, 0.01220703125000000000, 0.01269531250000000000, 0.01318359375000000000, 0.01367187500000000000, 0.01416015625000000000, 0.01464843750000000000, 0.01513671875000000000, 0.01562500000000000000, 0.01611328125000000000, 0.01660156250000000000, 0.01708984375000000000, 0.01757812500000000000, 0.01806640625000000000, 0.01855468750000000000, 0.01904296875000000000, 0.01953125000000000000, 0.02001953125000000000, 0.02050781250000000000, 0.02099609375000000000, 0.02148437500000000000, 0.02197265625000000000, 0.02246093750000000000, 0.02294921875000000000, 0.02343750000000000000, 0.02392578125000000347, 0.02441406250000000347, 0.02490234375000000347, 0.02539062500000000347, 0.02587890625000000347, 0.02636718750000000347, 0.02685546875000000347, 0.02734375000000000347, 0.02783203125000000347, 0.02832031250000000347, 0.02880859375000000347, 0.02929687500000000347, 0.02978515625000000347, 0.03027343750000000347, 0.03076171875000000347, 0.03125000000000000000, 0.03173828125000000000, 0.03222656250000000000, 0.03271484375000000000, 0.03320312500000000000, 0.03369140625000000000, 0.03417968750000000000, 0.03466796875000000000, 0.03515625000000000000, 0.03564453125000000000, 0.03613281250000000000, 0.03662109375000000000, 0.03710937500000000000, 0.03759765625000000000, 0.03808593750000000000, 0.03857421875000000000, 0.03906250000000000000, 0.03955078125000000000, 0.04003906250000000000, 0.04052734375000000000, 0.04101562500000000000, 0.04150390625000000000, 0.04199218750000000000, 0.04248046875000000000, 0.04296875000000000000, 0.04345703125000000000, 0.04394531250000000000, 0.04443359375000000000, 0.04492187500000000000, 0.04541015625000000000, 0.04589843750000000000, 0.04638671875000000000, 0.04687500000000000000, 0.04736328125000000694, 0.04785156250000000694, 0.04833984375000000694, 0.04882812500000000694, 0.04931640625000000694, 0.04980468750000000694, 0.05029296875000000694, 0.05078125000000000694, 0.05126953125000000694, 0.05175781250000000694, 0.05224609375000000694, 0.05273437500000000694, 0.05322265625000000694, 0.05371093750000000694, 0.05419921875000000694, 0.05468750000000000694, 0.05517578125000000694, 0.05566406250000000694, 0.05615234375000000694, 0.05664062500000000694, 0.05712890625000000694, 0.05761718750000000694, 0.05810546875000000694, 0.05859375000000000694, 0.05908203125000000694, 0.05957031250000000694, 0.06005859375000000694, 0.06054687500000000694, 0.06103515625000000694, 0.06152343750000000694, 0.06201171875000000694, 0.06250000000000000000, 0.06298828125000000000, 0.06347656250000000000, 0.06396484375000000000, 0.06445312500000000000, 0.06494140625000000000, 0.06542968750000000000, 0.06591796875000000000, 0.06640625000000000000, 0.06689453125000000000, 0.06738281250000000000, 0.06787109375000000000, 0.06835937500000000000, 0.06884765625000000000, 0.06933593750000000000, 0.06982421875000000000, 0.07031250000000000000, 0.07080078125000000000, 0.07128906250000000000, 0.07177734375000000000, 0.07226562500000000000, 0.07275390625000000000, 0.07324218750000000000, 0.07373046875000000000, 0.07421875000000000000, 0.07470703125000000000, 0.07519531250000000000, 0.07568359375000000000, 0.07617187500000000000, 0.07666015625000000000, 0.07714843750000000000, 0.07763671875000000000, 0.07812500000000000000, 0.07861328125000000000, 0.07910156250000000000, 0.07958984375000000000, 0.08007812500000000000, 0.08056640625000000000, 0.08105468750000000000, 0.08154296875000000000, 0.08203125000000000000, 0.08251953125000000000, 0.08300781250000000000, 0.08349609375000000000, 0.08398437500000000000, 0.08447265625000000000, 0.08496093750000000000, 0.08544921875000000000, 0.08593750000000000000, 0.08642578125000000000, 0.08691406250000000000, 0.08740234375000000000, 0.08789062500000000000, 0.08837890625000000000, 0.08886718750000000000, 0.08935546875000000000, 0.08984375000000000000, 0.09033203125000000000, 0.09082031250000000000, 0.09130859375000000000, 0.09179687500000000000, 0.09228515625000000000, 0.09277343750000000000, 0.09326171875000000000, 0.09375000000000000000, 0.09423828125000001388, 0.09472656250000001388, 0.09521484375000001388, 0.09570312500000001388, 0.09619140625000001388, 0.09667968750000001388, 0.09716796875000001388, 0.09765625000000001388, 0.09814453125000001388, 0.09863281250000001388, 0.09912109375000001388, 0.09960937500000001388, 0.1000976562500000139, 0.1005859375000000139, 0.1010742187500000139, 0.1015625000000000139, 0.1020507812500000139, 0.1025390625000000139, 0.1030273437500000139, 0.1035156250000000139, 0.1040039062500000139, 0.1044921875000000139, 0.1049804687500000139, 0.1054687500000000139, 0.1059570312500000139, 0.1064453125000000139, 0.1069335937500000139, 0.1074218750000000139, 0.1079101562500000139, 0.1083984375000000139, 0.1088867187500000139, 0.1093750000000000139, 0.1098632812500000139, 0.1103515625000000139, 0.1108398437500000139, 0.1113281250000000139, 0.1118164062500000139, 0.1123046875000000139, 0.1127929687500000139, 0.1132812500000000139, 0.1137695312500000139, 0.1142578125000000139, 0.1147460937500000139, 0.1152343750000000139, 0.1157226562500000139, 0.1162109375000000139, 0.1166992187500000139, 0.1171875000000000139, 0.1176757812500000139, 0.1181640625000000139, 0.1186523437500000139, 0.1191406250000000139, 0.1196289062500000139, 0.1201171875000000139, 0.1206054687500000139, 0.1210937500000000139, 0.1215820312500000139, 0.1220703125000000139, 0.1225585937500000139, 0.1230468750000000139, 0.1235351562500000139, 0.1240234375000000139, 0.1245117187500000139, 0.1250000000000000000, 0.1254882812500000000, 0.1259765625000000000, 0.1264648437500000000, 0.1269531250000000000, 0.1274414062500000000, 0.1279296875000000000, 0.1284179687500000000, 0.1289062500000000000, 0.1293945312500000000, 0.1298828125000000000, 0.1303710937500000000, 0.1308593750000000000, 0.1313476562500000000, 0.1318359375000000000, 0.1323242187500000000, 0.1328125000000000000, 0.1333007812500000000, 0.1337890625000000000, 0.1342773437500000000, 0.1347656250000000000, 0.1352539062500000000, 0.1357421875000000000, 0.1362304687500000000, 0.1367187500000000000, 0.1372070312500000000, 0.1376953125000000000, 0.1381835937500000000, 0.1386718750000000000, 0.1391601562500000000, 0.1396484375000000000, 0.1401367187500000000, 0.1406250000000000000, 0.1411132812500000000, 0.1416015625000000000, 0.1420898437500000000, 0.1425781250000000000, 0.1430664062500000000, 0.1435546875000000000, 0.1440429687500000000, 0.1445312500000000000, 0.1450195312500000000, 0.1455078125000000000, 0.1459960937500000000, 0.1464843750000000000, 0.1469726562500000000, 0.1474609375000000000, 0.1479492187500000000, 0.1484375000000000000, 0.1489257812500000000, 0.1494140625000000000, 0.1499023437500000000, 0.1503906250000000000, 0.1508789062500000000, 0.1513671875000000000, 0.1518554687500000000, 0.1523437500000000000, 0.1528320312500000000, 0.1533203125000000000, 0.1538085937500000000, 0.1542968750000000000, 0.1547851562500000000, 0.1552734375000000000, 0.1557617187500000000, 0.1562500000000000000, 0.1567382812500000000, 0.1572265625000000000, 0.1577148437500000000, 0.1582031250000000000, 0.1586914062500000000, 0.1591796875000000000, 0.1596679687500000000, 0.1601562500000000000, 0.1606445312500000000, 0.1611328125000000000, 0.1616210937500000000, 0.1621093750000000000, 0.1625976562500000000, 0.1630859375000000000, 0.1635742187500000000, 0.1640625000000000000, 0.1645507812500000000, 0.1650390625000000000, 0.1655273437500000000, 0.1660156250000000000, 0.1665039062500000000, 0.1669921875000000000, 0.1674804687500000000, 0.1679687500000000000, 0.1684570312500000000, 0.1689453125000000000, 0.1694335937500000000, 0.1699218750000000000, 0.1704101562500000000, 0.1708984375000000000, 0.1713867187500000000, 0.1718750000000000000, 0.1723632812500000000, 0.1728515625000000000, 0.1733398437500000000, 0.1738281250000000000, 0.1743164062500000000, 0.1748046875000000000, 0.1752929687500000000, 0.1757812500000000000, 0.1762695312500000000, 0.1767578125000000000, 0.1772460937500000000, 0.1777343750000000000, 0.1782226562500000000, 0.1787109375000000000, 0.1791992187500000000, 0.1796875000000000000, 0.1801757812500000000, 0.1806640625000000000, 0.1811523437500000000, 0.1816406250000000000, 0.1821289062500000000, 0.1826171875000000000, 0.1831054687500000000, 0.1835937500000000000, 0.1840820312500000000, 0.1845703125000000000, 0.1850585937500000000, 0.1855468750000000000, 0.1860351562500000000, 0.1865234375000000000, 0.1870117187500000000, 0.1875000000000000000, 0.1879882812500000278, 0.1884765625000000278, 0.1889648437500000278, 0.1894531250000000278, 0.1899414062500000278, 0.1904296875000000278, 0.1909179687500000278, 0.1914062500000000278, 0.1918945312500000278, 0.1923828125000000278, 0.1928710937500000278, 0.1933593750000000278, 0.1938476562500000278, 0.1943359375000000278, 0.1948242187500000278, 0.1953125000000000278, 0.1958007812500000278, 0.1962890625000000278, 0.1967773437500000278, 0.1972656250000000278, 0.1977539062500000278, 0.1982421875000000278, 0.1987304687500000278, 0.1992187500000000278, 0.1997070312500000278, 0.2001953125000000278, 0.2006835937500000278, 0.2011718750000000278, 0.2016601562500000278, 0.2021484375000000278, 0.2026367187500000278, 0.2031250000000000278, 0.2036132812500000278, 0.2041015625000000278, 0.2045898437500000278, 0.2050781250000000278, 0.2055664062500000278, 0.2060546875000000278, 0.2065429687500000278, 0.2070312500000000278, 0.2075195312500000278, 0.2080078125000000278, 0.2084960937500000278, 0.2089843750000000278, 0.2094726562500000278, 0.2099609375000000278, 0.2104492187500000278, 0.2109375000000000278, 0.2114257812500000278, 0.2119140625000000278, 0.2124023437500000278, 0.2128906250000000278, 0.2133789062500000278, 0.2138671875000000278, 0.2143554687500000278, 0.2148437500000000278, 0.2153320312500000278, 0.2158203125000000278, 0.2163085937500000278, 0.2167968750000000278, 0.2172851562500000278, 0.2177734375000000278, 0.2182617187500000278, 0.2187500000000000278, 0.2192382812500000278, 0.2197265625000000278, 0.2202148437500000278, 0.2207031250000000278, 0.2211914062500000278, 0.2216796875000000278, 0.2221679687500000278, 0.2226562500000000278, 0.2231445312500000278, 0.2236328125000000278, 0.2241210937500000278, 0.2246093750000000278, 0.2250976562500000278, 0.2255859375000000278, 0.2260742187500000278, 0.2265625000000000278, 0.2270507812500000278, 0.2275390625000000278, 0.2280273437500000278, 0.2285156250000000278, 0.2290039062500000278, 0.2294921875000000278, 0.2299804687500000278, 0.2304687500000000278, 0.2309570312500000278, 0.2314453125000000278, 0.2319335937500000278, 0.2324218750000000278, 0.2329101562500000278, 0.2333984375000000278, 0.2338867187500000278, 0.2343750000000000278, 0.2348632812500000278, 0.2353515625000000278, 0.2358398437500000278, 0.2363281250000000278, 0.2368164062500000278, 0.2373046875000000278, 0.2377929687500000278, 0.2382812500000000278, 0.2387695312500000278, 0.2392578125000000278, 0.2397460937500000278, 0.2402343750000000278, 0.2407226562500000278, 0.2412109375000000278, 0.2416992187500000278, 0.2421875000000000278, 0.2426757812500000278, 0.2431640625000000278, 0.2436523437500000278, 0.2441406250000000278, 0.2446289062500000278, 0.2451171875000000278, 0.2456054687500000278, 0.2460937500000000278, 0.2465820312500000278, 0.2470703125000000278, 0.2475585937500000278, 0.2480468750000000278, 0.2485351562500000278, 0.2490234375000000278, 0.2495117187500000278, 0.2500000000000000000, 0.2504882812500000000, 0.2509765625000000000, 0.2514648437500000000, 0.2519531250000000000, 0.2524414062500000000, 0.2529296875000000000, 0.2534179687500000000, 0.2539062500000000000, 0.2543945312500000000, 0.2548828125000000000, 0.2553710937500000000, 0.2558593750000000000, 0.2563476562500000000, 0.2568359375000000000, 0.2573242187500000000, 0.2578125000000000000, 0.2583007812500000000, 0.2587890625000000000, 0.2592773437500000000, 0.2597656250000000000, 0.2602539062500000000, 0.2607421875000000000, 0.2612304687500000000, 0.2617187500000000000, 0.2622070312500000000, 0.2626953125000000000, 0.2631835937500000000, 0.2636718750000000000, 0.2641601562500000000, 0.2646484375000000000, 0.2651367187500000000, 0.2656250000000000000, 0.2661132812500000000, 0.2666015625000000000, 0.2670898437500000000, 0.2675781250000000000, 0.2680664062500000000, 0.2685546875000000000, 0.2690429687500000000, 0.2695312500000000000, 0.2700195312500000000, 0.2705078125000000000, 0.2709960937500000000, 0.2714843750000000000, 0.2719726562500000000, 0.2724609375000000000, 0.2729492187500000000, 0.2734375000000000000, 0.2739257812500000000, 0.2744140625000000000, 0.2749023437500000000, 0.2753906250000000000, 0.2758789062500000000, 0.2763671875000000000, 0.2768554687500000000, 0.2773437500000000000, 0.2778320312500000000, 0.2783203125000000000, 0.2788085937500000000, 0.2792968750000000000, 0.2797851562500000000, 0.2802734375000000000, 0.2807617187500000000, 0.2812500000000000000, 0.2817382812500000000, 0.2822265625000000000, 0.2827148437500000000, 0.2832031250000000000, 0.2836914062500000000, 0.2841796875000000000, 0.2846679687500000000, 0.2851562500000000000, 0.2856445312500000000, 0.2861328125000000000, 0.2866210937500000000, 0.2871093750000000000, 0.2875976562500000000, 0.2880859375000000000, 0.2885742187500000000, 0.2890625000000000000, 0.2895507812500000000, 0.2900390625000000000, 0.2905273437500000000, 0.2910156250000000000, 0.2915039062500000000, 0.2919921875000000000, 0.2924804687500000000, 0.2929687500000000000, 0.2934570312500000000, 0.2939453125000000000, 0.2944335937500000000, 0.2949218750000000000, 0.2954101562500000000, 0.2958984375000000000, 0.2963867187500000000, 0.2968750000000000000, 0.2973632812500000000, 0.2978515625000000000, 0.2983398437500000000, 0.2988281250000000000, 0.2993164062500000000, 0.2998046875000000000, 0.3002929687500000000, 0.3007812500000000000, 0.3012695312500000000, 0.3017578125000000000, 0.3022460937500000000, 0.3027343750000000000, 0.3032226562500000000, 0.3037109375000000000, 0.3041992187500000000, 0.3046875000000000000, 0.3051757812500000000, 0.3056640625000000000, 0.3061523437500000000, 0.3066406250000000000, 0.3071289062500000000, 0.3076171875000000000, 0.3081054687500000000, 0.3085937500000000000, 0.3090820312500000000, 0.3095703125000000000, 0.3100585937500000000, 0.3105468750000000000, 0.3110351562500000000, 0.3115234375000000000, 0.3120117187500000000, 0.3125000000000000000, 0.3129882812500000000, 0.3134765625000000000, 0.3139648437500000000, 0.3144531250000000000, 0.3149414062500000000, 0.3154296875000000000, 0.3159179687500000000, 0.3164062500000000000, 0.3168945312500000000, 0.3173828125000000000, 0.3178710937500000000, 0.3183593750000000000, 0.3188476562500000000, 0.3193359375000000000, 0.3198242187500000000, 0.3203125000000000000, 0.3208007812500000000, 0.3212890625000000000, 0.3217773437500000000, 0.3222656250000000000, 0.3227539062500000000, 0.3232421875000000000, 0.3237304687500000000, 0.3242187500000000000, 0.3247070312500000000, 0.3251953125000000000, 0.3256835937500000000, 0.3261718750000000000, 0.3266601562500000000, 0.3271484375000000000, 0.3276367187500000000, 0.3281250000000000000, 0.3286132812500000000, 0.3291015625000000000, 0.3295898437500000000, 0.3300781250000000000, 0.3305664062500000000, 0.3310546875000000000, 0.3315429687500000000, 0.3320312500000000000, 0.3325195312500000000, 0.3330078125000000000, 0.3334960937500000000, 0.3339843750000000000, 0.3344726562500000000, 0.3349609375000000000, 0.3354492187500000000, 0.3359375000000000000, 0.3364257812500000000, 0.3369140625000000000, 0.3374023437500000000, 0.3378906250000000000, 0.3383789062500000000, 0.3388671875000000000, 0.3393554687500000000, 0.3398437500000000000, 0.3403320312500000000, 0.3408203125000000000, 0.3413085937500000000, 0.3417968750000000000, 0.3422851562500000000, 0.3427734375000000000, 0.3432617187500000000, 0.3437500000000000000, 0.3442382812500000000, 0.3447265625000000000, 0.3452148437500000000, 0.3457031250000000000, 0.3461914062500000000, 0.3466796875000000000, 0.3471679687500000000, 0.3476562500000000000, 0.3481445312500000000, 0.3486328125000000000, 0.3491210937500000000, 0.3496093750000000000, 0.3500976562500000000, 0.3505859375000000000, 0.3510742187500000000, 0.3515625000000000000, 0.3520507812500000000, 0.3525390625000000000, 0.3530273437500000000, 0.3535156250000000000, 0.3540039062500000000, 0.3544921875000000000, 0.3549804687500000000, 0.3554687500000000000, 0.3559570312500000000, 0.3564453125000000000, 0.3569335937500000000, 0.3574218750000000000, 0.3579101562500000000, 0.3583984375000000000, 0.3588867187500000000, 0.3593750000000000000, 0.3598632812500000000, 0.3603515625000000000, 0.3608398437500000000, 0.3613281250000000000, 0.3618164062500000000, 0.3623046875000000000, 0.3627929687500000000, 0.3632812500000000000, 0.3637695312500000000, 0.3642578125000000000, 0.3647460937500000000, 0.3652343750000000000, 0.3657226562500000000, 0.3662109375000000000, 0.3666992187500000000, 0.3671875000000000000, 0.3676757812500000000, 0.3681640625000000000, 0.3686523437500000000, 0.3691406250000000000, 0.3696289062500000000, 0.3701171875000000000, 0.3706054687500000000, 0.3710937500000000000, 0.3715820312500000000, 0.3720703125000000000, 0.3725585937500000000, 0.3730468750000000000, 0.3735351562500000000, 0.3740234375000000000, 0.3745117187500000000, 0.3750000000000000000, 0.3754882812500000555, 0.3759765625000000555, 0.3764648437500000555, 0.3769531250000000555, 0.3774414062500000555, 0.3779296875000000555, 0.3784179687500000555, 0.3789062500000000555, 0.3793945312500000555, 0.3798828125000000555, 0.3803710937500000555, 0.3808593750000000555, 0.3813476562500000555, 0.3818359375000000555, 0.3823242187500000555, 0.3828125000000000555, 0.3833007812500000555, 0.3837890625000000555, 0.3842773437500000555, 0.3847656250000000555, 0.3852539062500000555, 0.3857421875000000555, 0.3862304687500000555, 0.3867187500000000555, 0.3872070312500000555, 0.3876953125000000555, 0.3881835937500000555, 0.3886718750000000555, 0.3891601562500000555, 0.3896484375000000555, 0.3901367187500000555, 0.3906250000000000555, 0.3911132812500000555, 0.3916015625000000555, 0.3920898437500000555, 0.3925781250000000555, 0.3930664062500000555, 0.3935546875000000555, 0.3940429687500000555, 0.3945312500000000555, 0.3950195312500000555, 0.3955078125000000555, 0.3959960937500000555, 0.3964843750000000555, 0.3969726562500000555, 0.3974609375000000555, 0.3979492187500000555, 0.3984375000000000555, 0.3989257812500000555, 0.3994140625000000555, 0.3999023437500000555, 0.4003906250000000555, 0.4008789062500000555, 0.4013671875000000555, 0.4018554687500000555, 0.4023437500000000555, 0.4028320312500000555, 0.4033203125000000555, 0.4038085937500000555, 0.4042968750000000555, 0.4047851562500000555, 0.4052734375000000555, 0.4057617187500000555, 0.4062500000000000555, 0.4067382812500000555, 0.4072265625000000555, 0.4077148437500000555, 0.4082031250000000555, 0.4086914062500000555, 0.4091796875000000555, 0.4096679687500000555, 0.4101562500000000555, 0.4106445312500000555, 0.4111328125000000555, 0.4116210937500000555, 0.4121093750000000555, 0.4125976562500000555, 0.4130859375000000555, 0.4135742187500000555, 0.4140625000000000555, 0.4145507812500000555, 0.4150390625000000555, 0.4155273437500000555, 0.4160156250000000555, 0.4165039062500000555, 0.4169921875000000555, 0.4174804687500000555, 0.4179687500000000555, 0.4184570312500000555, 0.4189453125000000555, 0.4194335937500000555, 0.4199218750000000555, 0.4204101562500000555, 0.4208984375000000555, 0.4213867187500000555, 0.4218750000000000555, 0.4223632812500000555, 0.4228515625000000555, 0.4233398437500000555, 0.4238281250000000555, 0.4243164062500000555, 0.4248046875000000555, 0.4252929687500000555, 0.4257812500000000555, 0.4262695312500000555, 0.4267578125000000555, 0.4272460937500000555, 0.4277343750000000555, 0.4282226562500000555, 0.4287109375000000555, 0.4291992187500000555, 0.4296875000000000555, 0.4301757812500000555, 0.4306640625000000555, 0.4311523437500000555, 0.4316406250000000555, 0.4321289062500000555, 0.4326171875000000555, 0.4331054687500000555, 0.4335937500000000555, 0.4340820312500000555, 0.4345703125000000555, 0.4350585937500000555, 0.4355468750000000555, 0.4360351562500000555, 0.4365234375000000555, 0.4370117187500000555, 0.4375000000000000555, 0.4379882812500000555, 0.4384765625000000555, 0.4389648437500000555, 0.4394531250000000555, 0.4399414062500000555, 0.4404296875000000555, 0.4409179687500000555, 0.4414062500000000555, 0.4418945312500000555, 0.4423828125000000555, 0.4428710937500000555, 0.4433593750000000555, 0.4438476562500000555, 0.4443359375000000555, 0.4448242187500000555, 0.4453125000000000555, 0.4458007812500000555, 0.4462890625000000555, 0.4467773437500000555, 0.4472656250000000555, 0.4477539062500000555, 0.4482421875000000555, 0.4487304687500000555, 0.4492187500000000555, 0.4497070312500000555, 0.4501953125000000555, 0.4506835937500000555, 0.4511718750000000555, 0.4516601562500000555, 0.4521484375000000555, 0.4526367187500000555, 0.4531250000000000555, 0.4536132812500000555, 0.4541015625000000555, 0.4545898437500000555, 0.4550781250000000555, 0.4555664062500000555, 0.4560546875000000555, 0.4565429687500000555, 0.4570312500000000555, 0.4575195312500000555, 0.4580078125000000555, 0.4584960937500000555, 0.4589843750000000555, 0.4594726562500000555, 0.4599609375000000555, 0.4604492187500000555, 0.4609375000000000555, 0.4614257812500000555, 0.4619140625000000555, 0.4624023437500000555, 0.4628906250000000555, 0.4633789062500000555, 0.4638671875000000555, 0.4643554687500000555, 0.4648437500000000555, 0.4653320312500000555, 0.4658203125000000555, 0.4663085937500000555, 0.4667968750000000555, 0.4672851562500000555, 0.4677734375000000555, 0.4682617187500000555, 0.4687500000000000555, 0.4692382812500000555, 0.4697265625000000555, 0.4702148437500000555, 0.4707031250000000555, 0.4711914062500000555, 0.4716796875000000555, 0.4721679687500000555, 0.4726562500000000555, 0.4731445312500000555, 0.4736328125000000555, 0.4741210937500000555, 0.4746093750000000555, 0.4750976562500000555, 0.4755859375000000555, 0.4760742187500000555, 0.4765625000000000555, 0.4770507812500000555, 0.4775390625000000555, 0.4780273437500000555, 0.4785156250000000555, 0.4790039062500000555, 0.4794921875000000555, 0.4799804687500000555, 0.4804687500000000555, 0.4809570312500000555, 0.4814453125000000555, 0.4819335937500000555, 0.4824218750000000555, 0.4829101562500000555, 0.4833984375000000555, 0.4838867187500000555, 0.4843750000000000555, 0.4848632812500000555, 0.4853515625000000555, 0.4858398437500000555, 0.4863281250000000555, 0.4868164062500000555, 0.4873046875000000555, 0.4877929687500000555, 0.4882812500000000555, 0.4887695312500000555, 0.4892578125000000555, 0.4897460937500000555, 0.4902343750000000555, 0.4907226562500000555, 0.4912109375000000555, 0.4916992187500000555, 0.4921875000000000555, 0.4926757812500000555, 0.4931640625000000555, 0.4936523437500000555, 0.4941406250000000555, 0.4946289062500000555, 0.4951171875000000555, 0.4956054687500000555, 0.4960937500000000555, 0.4965820312500000555, 0.4970703125000000555, 0.4975585937500000555, 0.4980468750000000555, 0.4985351562500000555, 0.4990234375000000555, 0.4995117187500000555, 0.5000000000000000000, 0.5004882812500000000, 0.5009765625000000000, 0.5014648437500000000, 0.5019531250000000000, 0.5024414062500000000, 0.5029296875000000000, 0.5034179687500000000, 0.5039062500000000000, 0.5043945312500000000, 0.5048828125000000000, 0.5053710937500000000, 0.5058593750000000000, 0.5063476562500000000, 0.5068359375000000000, 0.5073242187500000000, 0.5078125000000000000, 0.5083007812500000000, 0.5087890625000000000, 0.5092773437500000000, 0.5097656250000000000, 0.5102539062500000000, 0.5107421875000000000, 0.5112304687500000000, 0.5117187500000000000, 0.5122070312500000000, 0.5126953125000000000, 0.5131835937500000000, 0.5136718750000000000, 0.5141601562500000000, 0.5146484375000000000, 0.5151367187500000000, 0.5156250000000000000, 0.5161132812500000000, 0.5166015625000000000, 0.5170898437500000000, 0.5175781250000000000, 0.5180664062500000000, 0.5185546875000000000, 0.5190429687500000000, 0.5195312500000000000, 0.5200195312500000000, 0.5205078125000000000, 0.5209960937500000000, 0.5214843750000000000, 0.5219726562500000000, 0.5224609375000000000, 0.5229492187500000000, 0.5234375000000000000, 0.5239257812500000000, 0.5244140625000000000, 0.5249023437500000000, 0.5253906250000000000, 0.5258789062500000000, 0.5263671875000000000, 0.5268554687500000000, 0.5273437500000000000, 0.5278320312500000000, 0.5283203125000000000, 0.5288085937500000000, 0.5292968750000000000, 0.5297851562500000000, 0.5302734375000000000, 0.5307617187500000000, 0.5312500000000000000, 0.5317382812500000000, 0.5322265625000000000, 0.5327148437500000000, 0.5332031250000000000, 0.5336914062500000000, 0.5341796875000000000, 0.5346679687500000000, 0.5351562500000000000, 0.5356445312500000000, 0.5361328125000000000, 0.5366210937500000000, 0.5371093750000000000, 0.5375976562500000000, 0.5380859375000000000, 0.5385742187500000000, 0.5390625000000000000, 0.5395507812500000000, 0.5400390625000000000, 0.5405273437500000000, 0.5410156250000000000, 0.5415039062500000000, 0.5419921875000000000, 0.5424804687500000000, 0.5429687500000000000, 0.5434570312500000000, 0.5439453125000000000, 0.5444335937500000000, 0.5449218750000000000, 0.5454101562500000000, 0.5458984375000000000, 0.5463867187500000000, 0.5468750000000000000, 0.5473632812500000000, 0.5478515625000000000, 0.5483398437500000000, 0.5488281250000000000, 0.5493164062500000000, 0.5498046875000000000, 0.5502929687500000000, 0.5507812500000000000, 0.5512695312500000000, 0.5517578125000000000, 0.5522460937500000000, 0.5527343750000000000, 0.5532226562500000000, 0.5537109375000000000, 0.5541992187500000000, 0.5546875000000000000, 0.5551757812500000000, 0.5556640625000000000, 0.5561523437500000000, 0.5566406250000000000, 0.5571289062500000000, 0.5576171875000000000, 0.5581054687500000000, 0.5585937500000000000, 0.5590820312500000000, 0.5595703125000000000, 0.5600585937500000000, 0.5605468750000000000, 0.5610351562500000000, 0.5615234375000000000, 0.5620117187500000000, 0.5625000000000000000, 0.5629882812500000000, 0.5634765625000000000, 0.5639648437500000000, 0.5644531250000000000, 0.5649414062500000000, 0.5654296875000000000, 0.5659179687500000000, 0.5664062500000000000, 0.5668945312500000000, 0.5673828125000000000, 0.5678710937500000000, 0.5683593750000000000, 0.5688476562500000000, 0.5693359375000000000, 0.5698242187500000000, 0.5703125000000000000, 0.5708007812500000000, 0.5712890625000000000, 0.5717773437500000000, 0.5722656250000000000, 0.5727539062500000000, 0.5732421875000000000, 0.5737304687500000000, 0.5742187500000000000, 0.5747070312500000000, 0.5751953125000000000, 0.5756835937500000000, 0.5761718750000000000, 0.5766601562500000000, 0.5771484375000000000, 0.5776367187500000000, 0.5781250000000000000, 0.5786132812500000000, 0.5791015625000000000, 0.5795898437500000000, 0.5800781250000000000, 0.5805664062500000000, 0.5810546875000000000, 0.5815429687500000000, 0.5820312500000000000, 0.5825195312500000000, 0.5830078125000000000, 0.5834960937500000000, 0.5839843750000000000, 0.5844726562500000000, 0.5849609375000000000, 0.5854492187500000000, 0.5859375000000000000, 0.5864257812500000000, 0.5869140625000000000, 0.5874023437500000000, 0.5878906250000000000, 0.5883789062500000000, 0.5888671875000000000, 0.5893554687500000000, 0.5898437500000000000, 0.5903320312500000000, 0.5908203125000000000, 0.5913085937500000000, 0.5917968750000000000, 0.5922851562500000000, 0.5927734375000000000, 0.5932617187500000000, 0.5937500000000000000, 0.5942382812500000000, 0.5947265625000000000, 0.5952148437500000000, 0.5957031250000000000, 0.5961914062500000000, 0.5966796875000000000, 0.5971679687500000000, 0.5976562500000000000, 0.5981445312500000000, 0.5986328125000000000, 0.5991210937500000000, 0.5996093750000000000, 0.6000976562500000000, 0.6005859375000000000, 0.6010742187500000000, 0.6015625000000000000, 0.6020507812500000000, 0.6025390625000000000, 0.6030273437500000000, 0.6035156250000000000, 0.6040039062500000000, 0.6044921875000000000, 0.6049804687500000000, 0.6054687500000000000, 0.6059570312500000000, 0.6064453125000000000, 0.6069335937500000000, 0.6074218750000000000, 0.6079101562500000000, 0.6083984375000000000, 0.6088867187500000000, 0.6093750000000000000, 0.6098632812500000000, 0.6103515625000000000, 0.6108398437500000000, 0.6113281250000000000, 0.6118164062500000000, 0.6123046875000000000, 0.6127929687500000000, 0.6132812500000000000, 0.6137695312500000000, 0.6142578125000000000, 0.6147460937500000000, 0.6152343750000000000, 0.6157226562500000000, 0.6162109375000000000, 0.6166992187500000000, 0.6171875000000000000, 0.6176757812500000000, 0.6181640625000000000, 0.6186523437500000000, 0.6191406250000000000, 0.6196289062500000000, 0.6201171875000000000, 0.6206054687500000000, 0.6210937500000000000, 0.6215820312500000000, 0.6220703125000000000, 0.6225585937500000000, 0.6230468750000000000, 0.6235351562500000000, 0.6240234375000000000, 0.6245117187500000000, 0.6250000000000000000, 0.6254882812500000000, 0.6259765625000000000, 0.6264648437500000000, 0.6269531250000000000, 0.6274414062500000000, 0.6279296875000000000, 0.6284179687500000000, 0.6289062500000000000, 0.6293945312500000000, 0.6298828125000000000, 0.6303710937500000000, 0.6308593750000000000, 0.6313476562500000000, 0.6318359375000000000, 0.6323242187500000000, 0.6328125000000000000, 0.6333007812500000000, 0.6337890625000000000, 0.6342773437500000000, 0.6347656250000000000, 0.6352539062500000000, 0.6357421875000000000, 0.6362304687500000000, 0.6367187500000000000, 0.6372070312500000000, 0.6376953125000000000, 0.6381835937500000000, 0.6386718750000000000, 0.6391601562500000000, 0.6396484375000000000, 0.6401367187500000000, 0.6406250000000000000, 0.6411132812500000000, 0.6416015625000000000, 0.6420898437500000000, 0.6425781250000000000, 0.6430664062500000000, 0.6435546875000000000, 0.6440429687500000000, 0.6445312500000000000, 0.6450195312500000000, 0.6455078125000000000, 0.6459960937500000000, 0.6464843750000000000, 0.6469726562500000000, 0.6474609375000000000, 0.6479492187500000000, 0.6484375000000000000, 0.6489257812500000000, 0.6494140625000000000, 0.6499023437500000000, 0.6503906250000000000, 0.6508789062500000000, 0.6513671875000000000, 0.6518554687500000000, 0.6523437500000000000, 0.6528320312500000000, 0.6533203125000000000, 0.6538085937500000000, 0.6542968750000000000, 0.6547851562500000000, 0.6552734375000000000, 0.6557617187500000000, 0.6562500000000000000, 0.6567382812500000000, 0.6572265625000000000, 0.6577148437500000000, 0.6582031250000000000, 0.6586914062500000000, 0.6591796875000000000, 0.6596679687500000000, 0.6601562500000000000, 0.6606445312500000000, 0.6611328125000000000, 0.6616210937500000000, 0.6621093750000000000, 0.6625976562500000000, 0.6630859375000000000, 0.6635742187500000000, 0.6640625000000000000, 0.6645507812500000000, 0.6650390625000000000, 0.6655273437500000000, 0.6660156250000000000, 0.6665039062500000000, 0.6669921875000000000, 0.6674804687500000000, 0.6679687500000000000, 0.6684570312500000000, 0.6689453125000000000, 0.6694335937500000000, 0.6699218750000000000, 0.6704101562500000000, 0.6708984375000000000, 0.6713867187500000000, 0.6718750000000000000, 0.6723632812500000000, 0.6728515625000000000, 0.6733398437500000000, 0.6738281250000000000, 0.6743164062500000000, 0.6748046875000000000, 0.6752929687500000000, 0.6757812500000000000, 0.6762695312500000000, 0.6767578125000000000, 0.6772460937500000000, 0.6777343750000000000, 0.6782226562500000000, 0.6787109375000000000, 0.6791992187500000000, 0.6796875000000000000, 0.6801757812500000000, 0.6806640625000000000, 0.6811523437500000000, 0.6816406250000000000, 0.6821289062500000000, 0.6826171875000000000, 0.6831054687500000000, 0.6835937500000000000, 0.6840820312500000000, 0.6845703125000000000, 0.6850585937500000000, 0.6855468750000000000, 0.6860351562500000000, 0.6865234375000000000, 0.6870117187500000000, 0.6875000000000000000, 0.6879882812500000000, 0.6884765625000000000, 0.6889648437500000000, 0.6894531250000000000, 0.6899414062500000000, 0.6904296875000000000, 0.6909179687500000000, 0.6914062500000000000, 0.6918945312500000000, 0.6923828125000000000, 0.6928710937500000000, 0.6933593750000000000, 0.6938476562500000000, 0.6943359375000000000, 0.6948242187500000000, 0.6953125000000000000, 0.6958007812500000000, 0.6962890625000000000, 0.6967773437500000000, 0.6972656250000000000, 0.6977539062500000000, 0.6982421875000000000, 0.6987304687500000000, 0.6992187500000000000, 0.6997070312500000000, 0.7001953125000000000, 0.7006835937500000000, 0.7011718750000000000, 0.7016601562500000000, 0.7021484375000000000, 0.7026367187500000000, 0.7031250000000000000, 0.7036132812500000000, 0.7041015625000000000, 0.7045898437500000000, 0.7050781250000000000, 0.7055664062500000000, 0.7060546875000000000, 0.7065429687500000000, 0.7070312500000000000, 0.7075195312500000000, 0.7080078125000000000, 0.7084960937500000000, 0.7089843750000000000, 0.7094726562500000000, 0.7099609375000000000, 0.7104492187500000000, 0.7109375000000000000, 0.7114257812500000000, 0.7119140625000000000, 0.7124023437500000000, 0.7128906250000000000, 0.7133789062500000000, 0.7138671875000000000, 0.7143554687500000000, 0.7148437500000000000, 0.7153320312500000000, 0.7158203125000000000, 0.7163085937500000000, 0.7167968750000000000, 0.7172851562500000000, 0.7177734375000000000, 0.7182617187500000000, 0.7187500000000000000, 0.7192382812500000000, 0.7197265625000000000, 0.7202148437500000000, 0.7207031250000000000, 0.7211914062500000000, 0.7216796875000000000, 0.7221679687500000000, 0.7226562500000000000, 0.7231445312500000000, 0.7236328125000000000, 0.7241210937500000000, 0.7246093750000000000, 0.7250976562500000000, 0.7255859375000000000, 0.7260742187500000000, 0.7265625000000000000, 0.7270507812500000000, 0.7275390625000000000, 0.7280273437500000000, 0.7285156250000000000, 0.7290039062500000000, 0.7294921875000000000, 0.7299804687500000000, 0.7304687500000000000, 0.7309570312500000000, 0.7314453125000000000, 0.7319335937500000000, 0.7324218750000000000, 0.7329101562500000000, 0.7333984375000000000, 0.7338867187500000000, 0.7343750000000000000, 0.7348632812500000000, 0.7353515625000000000, 0.7358398437500000000, 0.7363281250000000000, 0.7368164062500000000, 0.7373046875000000000, 0.7377929687500000000, 0.7382812500000000000, 0.7387695312500000000, 0.7392578125000000000, 0.7397460937500000000, 0.7402343750000000000, 0.7407226562500000000, 0.7412109375000000000, 0.7416992187500000000, 0.7421875000000000000, 0.7426757812500000000, 0.7431640625000000000, 0.7436523437500000000, 0.7441406250000000000, 0.7446289062500000000, 0.7451171875000000000, 0.7456054687500000000, 0.7460937500000000000, 0.7465820312500000000, 0.7470703125000000000, 0.7475585937500000000, 0.7480468750000000000, 0.7485351562500000000, 0.7490234375000000000, 0.7495117187500000000, 0.7500000000000000000, 0.7504882812500001110, 0.7509765625000001110, 0.7514648437500001110, 0.7519531250000001110, 0.7524414062500001110, 0.7529296875000001110, 0.7534179687500001110, 0.7539062500000001110, 0.7543945312500001110, 0.7548828125000001110, 0.7553710937500001110, 0.7558593750000001110, 0.7563476562500001110, 0.7568359375000001110, 0.7573242187500001110, 0.7578125000000001110, 0.7583007812500001110, 0.7587890625000001110, 0.7592773437500001110, 0.7597656250000001110, 0.7602539062500001110, 0.7607421875000001110, 0.7612304687500001110, 0.7617187500000001110, 0.7622070312500001110, 0.7626953125000001110, 0.7631835937500001110, 0.7636718750000001110, 0.7641601562500001110, 0.7646484375000001110, 0.7651367187500001110, 0.7656250000000001110, 0.7661132812500001110, 0.7666015625000001110, 0.7670898437500001110, 0.7675781250000001110, 0.7680664062500001110, 0.7685546875000001110, 0.7690429687500001110, 0.7695312500000001110, 0.7700195312500001110, 0.7705078125000001110, 0.7709960937500001110, 0.7714843750000001110, 0.7719726562500001110, 0.7724609375000001110, 0.7729492187500001110, 0.7734375000000001110, 0.7739257812500001110, 0.7744140625000001110, 0.7749023437500001110, 0.7753906250000001110, 0.7758789062500001110, 0.7763671875000001110, 0.7768554687500001110, 0.7773437500000001110, 0.7778320312500001110, 0.7783203125000001110, 0.7788085937500001110, 0.7792968750000001110, 0.7797851562500001110, 0.7802734375000001110, 0.7807617187500001110, 0.7812500000000001110, 0.7817382812500001110, 0.7822265625000001110, 0.7827148437500001110, 0.7832031250000001110, 0.7836914062500001110, 0.7841796875000001110, 0.7846679687500001110, 0.7851562500000001110, 0.7856445312500001110, 0.7861328125000001110, 0.7866210937500001110, 0.7871093750000001110, 0.7875976562500001110, 0.7880859375000001110, 0.7885742187500001110, 0.7890625000000001110, 0.7895507812500001110, 0.7900390625000001110, 0.7905273437500001110, 0.7910156250000001110, 0.7915039062500001110, 0.7919921875000001110, 0.7924804687500001110, 0.7929687500000001110, 0.7934570312500001110, 0.7939453125000001110, 0.7944335937500001110, 0.7949218750000001110, 0.7954101562500001110, 0.7958984375000001110, 0.7963867187500001110, 0.7968750000000001110, 0.7973632812500001110, 0.7978515625000001110, 0.7983398437500001110, 0.7988281250000001110, 0.7993164062500001110, 0.7998046875000001110, 0.8002929687500001110, 0.8007812500000001110, 0.8012695312500001110, 0.8017578125000001110, 0.8022460937500001110, 0.8027343750000001110, 0.8032226562500001110, 0.8037109375000001110, 0.8041992187500001110, 0.8046875000000001110, 0.8051757812500001110, 0.8056640625000001110, 0.8061523437500001110, 0.8066406250000001110, 0.8071289062500001110, 0.8076171875000001110, 0.8081054687500001110, 0.8085937500000001110, 0.8090820312500001110, 0.8095703125000001110, 0.8100585937500001110, 0.8105468750000001110, 0.8110351562500001110, 0.8115234375000001110, 0.8120117187500001110, 0.8125000000000001110, 0.8129882812500001110, 0.8134765625000001110, 0.8139648437500001110, 0.8144531250000001110, 0.8149414062500001110, 0.8154296875000001110, 0.8159179687500001110, 0.8164062500000001110, 0.8168945312500001110, 0.8173828125000001110, 0.8178710937500001110, 0.8183593750000001110, 0.8188476562500001110, 0.8193359375000001110, 0.8198242187500001110, 0.8203125000000001110, 0.8208007812500001110, 0.8212890625000001110, 0.8217773437500001110, 0.8222656250000001110, 0.8227539062500001110, 0.8232421875000001110, 0.8237304687500001110, 0.8242187500000001110, 0.8247070312500001110, 0.8251953125000001110, 0.8256835937500001110, 0.8261718750000001110, 0.8266601562500001110, 0.8271484375000001110, 0.8276367187500001110, 0.8281250000000001110, 0.8286132812500001110, 0.8291015625000001110, 0.8295898437500001110, 0.8300781250000001110, 0.8305664062500001110, 0.8310546875000001110, 0.8315429687500001110, 0.8320312500000001110, 0.8325195312500001110, 0.8330078125000001110, 0.8334960937500001110, 0.8339843750000001110, 0.8344726562500001110, 0.8349609375000001110, 0.8354492187500001110, 0.8359375000000001110, 0.8364257812500001110, 0.8369140625000001110, 0.8374023437500001110, 0.8378906250000001110, 0.8383789062500001110, 0.8388671875000001110, 0.8393554687500001110, 0.8398437500000001110, 0.8403320312500001110, 0.8408203125000001110, 0.8413085937500001110, 0.8417968750000001110, 0.8422851562500001110, 0.8427734375000001110, 0.8432617187500001110, 0.8437500000000001110, 0.8442382812500001110, 0.8447265625000001110, 0.8452148437500001110, 0.8457031250000001110, 0.8461914062500001110, 0.8466796875000001110, 0.8471679687500001110, 0.8476562500000001110, 0.8481445312500001110, 0.8486328125000001110, 0.8491210937500001110, 0.8496093750000001110, 0.8500976562500001110, 0.8505859375000001110, 0.8510742187500001110, 0.8515625000000001110, 0.8520507812500001110, 0.8525390625000001110, 0.8530273437500001110, 0.8535156250000001110, 0.8540039062500001110, 0.8544921875000001110, 0.8549804687500001110, 0.8554687500000001110, 0.8559570312500001110, 0.8564453125000001110, 0.8569335937500001110, 0.8574218750000001110, 0.8579101562500001110, 0.8583984375000001110, 0.8588867187500001110, 0.8593750000000001110, 0.8598632812500001110, 0.8603515625000001110, 0.8608398437500001110, 0.8613281250000001110, 0.8618164062500001110, 0.8623046875000001110, 0.8627929687500001110, 0.8632812500000001110, 0.8637695312500001110, 0.8642578125000001110, 0.8647460937500001110, 0.8652343750000001110, 0.8657226562500001110, 0.8662109375000001110, 0.8666992187500001110, 0.8671875000000001110, 0.8676757812500001110, 0.8681640625000001110, 0.8686523437500001110, 0.8691406250000001110, 0.8696289062500001110, 0.8701171875000001110, 0.8706054687500001110, 0.8710937500000001110, 0.8715820312500001110, 0.8720703125000001110, 0.8725585937500001110, 0.8730468750000001110, 0.8735351562500001110, 0.8740234375000001110, 0.8745117187500001110, 0.8750000000000001110, 0.8754882812500001110, 0.8759765625000001110, 0.8764648437500001110, 0.8769531250000001110, 0.8774414062500001110, 0.8779296875000001110, 0.8784179687500001110, 0.8789062500000001110, 0.8793945312500001110, 0.8798828125000001110, 0.8803710937500001110, 0.8808593750000001110, 0.8813476562500001110, 0.8818359375000001110, 0.8823242187500001110, 0.8828125000000001110, 0.8833007812500001110, 0.8837890625000001110, 0.8842773437500001110, 0.8847656250000001110, 0.8852539062500001110, 0.8857421875000001110, 0.8862304687500001110, 0.8867187500000001110, 0.8872070312500001110, 0.8876953125000001110, 0.8881835937500001110, 0.8886718750000001110, 0.8891601562500001110, 0.8896484375000001110, 0.8901367187500001110, 0.8906250000000001110, 0.8911132812500001110, 0.8916015625000001110, 0.8920898437500001110, 0.8925781250000001110, 0.8930664062500001110, 0.8935546875000001110, 0.8940429687500001110, 0.8945312500000001110, 0.8950195312500001110, 0.8955078125000001110, 0.8959960937500001110, 0.8964843750000001110, 0.8969726562500001110, 0.8974609375000001110, 0.8979492187500001110, 0.8984375000000001110, 0.8989257812500001110, 0.8994140625000001110, 0.8999023437500001110, 0.9003906250000001110, 0.9008789062500001110, 0.9013671875000001110, 0.9018554687500001110, 0.9023437500000001110, 0.9028320312500001110, 0.9033203125000001110, 0.9038085937500001110, 0.9042968750000001110, 0.9047851562500001110, 0.9052734375000001110, 0.9057617187500001110, 0.9062500000000001110, 0.9067382812500001110, 0.9072265625000001110, 0.9077148437500001110, 0.9082031250000001110, 0.9086914062500001110, 0.9091796875000001110, 0.9096679687500001110, 0.9101562500000001110, 0.9106445312500001110, 0.9111328125000001110, 0.9116210937500001110, 0.9121093750000001110, 0.9125976562500001110, 0.9130859375000001110, 0.9135742187500001110, 0.9140625000000001110, 0.9145507812500001110, 0.9150390625000001110, 0.9155273437500001110, 0.9160156250000001110, 0.9165039062500001110, 0.9169921875000001110, 0.9174804687500001110, 0.9179687500000001110, 0.9184570312500001110, 0.9189453125000001110, 0.9194335937500001110, 0.9199218750000001110, 0.9204101562500001110, 0.9208984375000001110, 0.9213867187500001110, 0.9218750000000001110, 0.9223632812500001110, 0.9228515625000001110, 0.9233398437500001110, 0.9238281250000001110, 0.9243164062500001110, 0.9248046875000001110, 0.9252929687500001110, 0.9257812500000001110, 0.9262695312500001110, 0.9267578125000001110, 0.9272460937500001110, 0.9277343750000001110, 0.9282226562500001110, 0.9287109375000001110, 0.9291992187500001110, 0.9296875000000001110, 0.9301757812500001110, 0.9306640625000001110, 0.9311523437500001110, 0.9316406250000001110, 0.9321289062500001110, 0.9326171875000001110, 0.9331054687500001110, 0.9335937500000001110, 0.9340820312500001110, 0.9345703125000001110, 0.9350585937500001110, 0.9355468750000001110, 0.9360351562500001110, 0.9365234375000001110, 0.9370117187500001110, 0.9375000000000001110, 0.9379882812500001110, 0.9384765625000001110, 0.9389648437500001110, 0.9394531250000001110, 0.9399414062500001110, 0.9404296875000001110, 0.9409179687500001110, 0.9414062500000001110, 0.9418945312500001110, 0.9423828125000001110, 0.9428710937500001110, 0.9433593750000001110, 0.9438476562500001110, 0.9443359375000001110, 0.9448242187500001110, 0.9453125000000001110, 0.9458007812500001110, 0.9462890625000001110, 0.9467773437500001110, 0.9472656250000001110, 0.9477539062500001110, 0.9482421875000001110, 0.9487304687500001110, 0.9492187500000001110, 0.9497070312500001110, 0.9501953125000001110, 0.9506835937500001110, 0.9511718750000001110, 0.9516601562500001110, 0.9521484375000001110, 0.9526367187500001110, 0.9531250000000001110, 0.9536132812500001110, 0.9541015625000001110, 0.9545898437500001110, 0.9550781250000001110, 0.9555664062500001110, 0.9560546875000001110, 0.9565429687500001110, 0.9570312500000001110, 0.9575195312500001110, 0.9580078125000001110, 0.9584960937500001110, 0.9589843750000001110, 0.9594726562500001110, 0.9599609375000001110, 0.9604492187500001110, 0.9609375000000001110, 0.9614257812500001110, 0.9619140625000001110, 0.9624023437500001110, 0.9628906250000001110, 0.9633789062500001110, 0.9638671875000001110, 0.9643554687500001110, 0.9648437500000001110, 0.9653320312500001110, 0.9658203125000001110, 0.9663085937500001110, 0.9667968750000001110, 0.9672851562500001110, 0.9677734375000001110, 0.9682617187500001110, 0.9687500000000001110, 0.9692382812500001110, 0.9697265625000001110, 0.9702148437500001110, 0.9707031250000001110, 0.9711914062500001110, 0.9716796875000001110, 0.9721679687500001110, 0.9726562500000001110, 0.9731445312500001110, 0.9736328125000001110, 0.9741210937500001110, 0.9746093750000001110, 0.9750976562500001110, 0.9755859375000001110, 0.9760742187500001110, 0.9765625000000001110, 0.9770507812500001110, 0.9775390625000001110, 0.9780273437500001110, 0.9785156250000001110, 0.9790039062500001110, 0.9794921875000001110, 0.9799804687500001110, 0.9804687500000001110, 0.9809570312500001110, 0.9814453125000001110, 0.9819335937500001110, 0.9824218750000001110, 0.9829101562500001110, 0.9833984375000001110, 0.9838867187500001110, 0.9843750000000001110, 0.9848632812500001110, 0.9853515625000001110, 0.9858398437500001110, 0.9863281250000001110, 0.9868164062500001110, 0.9873046875000001110, 0.9877929687500001110, 0.9882812500000001110, 0.9887695312500001110, 0.9892578125000001110, 0.9897460937500001110, 0.9902343750000001110, 0.9907226562500001110, 0.9912109375000001110, 0.9916992187500001110, 0.9921875000000001110, 0.9926757812500001110, 0.9931640625000001110, 0.9936523437500001110, 0.9941406250000001110, 0.9946289062500001110, 0.9951171875000001110, 0.9956054687500001110, 0.9960937500000001110, 0.9965820312500001110, 0.9970703125000001110, 0.9975585937500001110, 0.9980468750000001110, 0.9985351562500001110, 0.9990234375000001110, 0.9995117187500001110, 1.000000000000000000 ),
 ( 0.000000000000000000, 1.000000000000000000 ),
 .UNSPECIFIED. ) ;
#70298=CARTESIAN_POINT ( 'NONE',  ( -58.52287095715006870, -23.72773821059536914, 11.05748984161097326 ) ) ;
#70299=ADVANCED_FACE ( 'NONE', ( #82861 ), #89555, .T. ) ;
#70300=CARTESIAN_POINT ( 'NONE',  ( -20.02981537788295441, -6.213780249082809348, -1.500000000000002220 ) ) ;
#70305=LINE ( 'NONE', #75903, #100383 ) ;
#70306=CARTESIAN_POINT ( 'NONE',  ( -59.63220076935764524, -24.34968618360933235, 0.1864209137778795600 ) ) ;
#70308=CARTESIAN_POINT ( 'NONE',  ( -22.11311035156252558, 1.696007508605793301, 11.49999999999999645 ) ) ;
#70309=VERTEX_POINT ( 'NONE', #21449 ) ;
#70313=VECTOR ( 'NONE', #38163, 1000.000000000000114 ) ;
#70314=CARTESIAN_POINT ( 'NONE',  ( -12.01393383709116947, -19.22582291892495121, -1.500000000000002220 ) ) ;
#70315=CARTESIAN_POINT ( 'NONE',  ( -28.24880736952684046, -24.86983583622034644, 7.480645431890892816 ) ) ;
#70316=ORIENTED_EDGE ( 'NONE', *, *, #43625, .F. ) ;
#70317=VECTOR ( 'NONE', #48631, 1000.000000000000114 ) ;
#70318=ORIENTED_EDGE ( 'NONE', *, *, #63532, .T. ) ;
#70320=CARTESIAN_POINT ( 'NONE',  ( -7.946508460909448956, -18.53024980520100939, 11.49999999999998934 ) ) ;
#70324=CARTESIAN_POINT ( 'NONE',  ( 16.55124408090292576, 15.08944307983326638, -1.500000000000002220 ) ) ;
#70325=ORIENTED_EDGE ( 'NONE', *, *, #62083, .T. ) ;
#70326=ORIENTED_EDGE ( 'NONE', *, *, #97731, .T. ) ;
#70329=DIRECTION ( 'NONE',  ( -3.773278334453079618E-23, 0.9999999999976377785, 2.173523156925979975E-06 ) ) ;
#70330=CARTESIAN_POINT ( 'NONE',  ( -116.5228709571500616, -23.47596703998600631, 11.44779298504227860 ) ) ;
#70331=FACE_BOUND ( 'NONE', #81527, .T. ) ;
#70333=CARTESIAN_POINT ( 'NONE',  ( -19.49195742049215241, -1.735909528584683947, -1.500000000000002220 ) ) ;
#70335=CARTESIAN_POINT ( 'NONE',  ( -4.253298834618286506, 21.06115358058179154, 11.49999999999998934 ) ) ;
#70336=DIRECTION ( 'NONE',  ( 0.000000000000000000, -2.173523156925979552E-06, 0.9999999999976378895 ) ) ;
#70338=CARTESIAN_POINT ( 'NONE',  ( -68.52287095715006160, -29.50248528299804818, 1.056150453629036701 ) ) ;
#70340=CARTESIAN_POINT ( 'NONE',  ( -68.62287095715004170, -24.50321055353803601, 9.387540953477524042 ) ) ;
#70341=CARTESIAN_POINT ( 'NONE',  ( 21.82588152991271713, 6.770963248321698380, -1.500000000000002220 ) ) ;
#70343=CARTESIAN_POINT ( 'NONE',  ( -124.6228709571500559, -24.64965695001469115, 8.947790433994175174 ) ) ;
#70344=CARTESIAN_POINT ( 'NONE',  ( -53.50785965996792726, -23.96119346886879953, -0.6495511937832126881 ) ) ;
#70345=CARTESIAN_POINT ( 'NONE',  ( 0.1258803491696451060, 20.03332480481931199, 11.49999999999999645 ) ) ;
#70346=CARTESIAN_POINT ( 'NONE',  ( -100.5228709571500758, -23.47593901973090524, -1.443836447538996648 ) ) ;
#70347=CARTESIAN_POINT ( 'NONE',  ( -107.6228709571500701, -24.64898659630368272, 1.056161002820831474 ) ) ;
#70348=CARTESIAN_POINT ( 'NONE',  ( -53.52287095715006870, -24.64965694238574656, 8.947790433994203596 ) ) ;
#70351=CARTESIAN_POINT ( 'NONE',  ( -85.62287095715008434, -23.84047902841601640, -0.8780736468305717635 ) ) ;
#70352=CARTESIAN_POINT ( 'NONE',  ( -19.76859095128058996, -9.124614402804876789, -1.500000000000002220 ) ) ;
#70354=CARTESIAN_POINT ( 'NONE',  ( -8.027368788987615744, 17.96763083595211441, -1.500000000000002220 ) ) ;
#70355=PLANE ( 'NONE',  #78217 ) ;
#70356=B_SPLINE_CURVE_WITH_KNOTS ( 'NONE', 3,
 ( #99882, #59863, #98394, #45629 ),
 .UNSPECIFIED., .F., .F.,
 ( 4, 4 ),
 ( 0.9804860655770837319, 0.9894924968491983774 ),
 .UNSPECIFIED. ) ;
#70357=CARTESIAN_POINT ( 'NONE',  ( -109.6940667814372006, -25.27925840780774536, 5.011372401766285734 ) ) ;
#70360=CARTESIAN_POINT ( 'NONE',  ( -39.29876498011696384, -25.30691688891204905, 5.130634121476438381 ) ) ;
#70361=CARTESIAN_POINT ( 'NONE',  ( -4.563637348303267949, -20.04915943051449645, 11.49999999999999645 ) ) ;
#70363=CARTESIAN_POINT ( 'NONE',  ( -120.5922450961300143, -23.85016227208581441, -0.8807180028928249804 ) ) ;
#70364=CARTESIAN_POINT ( 'NONE',  ( 6.494847429386178206, -21.66115869805930672, 11.49999999999999645 ) ) ;
#70366=CARTESIAN_POINT ( 'NONE',  ( -80.88924702628075636, -25.30869131066464561, 4.592921213095906730 ) ) ;
#70368=CARTESIAN_POINT ( 'NONE',  ( -125.6241953133450409, -24.63419186844610920, 9.035850630976920428 ) ) ;
#70370=DIRECTION ( 'NONE',  ( -3.773278334453080206E-23, 0.9999999999976377785, 2.173523156925979975E-06 ) ) ;
#70373=B_SPLINE_CURVE_WITH_KNOTS ( 'NONE', 3,
 ( #18297, #9174, #40135, #40640 ),
 .UNSPECIFIED., .F., .F.,
 ( 4, 4 ),
 ( 0.000000000000000000, 0.0005192307692307995826 ),
 .UNSPECIFIED. ) ;
#70375=CARTESIAN_POINT ( 'NONE',  ( -22.22199965279648737, -6.226755796435518242, 11.49999999999999645 ) ) ;
#70376=CARTESIAN_POINT ( 'NONE',  ( 10.87194125936840194, 20.03610521102953257, -1.500000000000002220 ) ) ;
#70378=CARTESIAN_POINT ( 'NONE',  ( -96.51886588111300114, -23.73766607897670511, -1.055555164236452681 ) ) ;
#70379=CARTESIAN_POINT ( 'NONE',  ( -86.52287095715006160, -23.47596703998600631, 11.44779298504228393 ) ) ;
#70380=CARTESIAN_POINT ( 'NONE',  ( 22.31695869535024102, -2.478243017838637652, 11.49999999999999645 ) ) ;
#70381=ORIENTED_EDGE ( 'NONE', *, *, #50856, .F. ) ;
#70382=CARTESIAN_POINT ( 'NONE',  ( -106.5228709571500758, -24.64898659630368627, 1.056161002820831474 ) ) ;
#70383=CARTESIAN_POINT ( 'NONE',  ( -34.62287095715007013, -24.50321055353804311, 9.387540953477543582 ) ) ;
#70384=CARTESIAN_POINT ( 'NONE',  ( 21.59112034314636119, 3.954845139028329015, -1.500000000000002220 ) ) ;
#70386=CARTESIAN_POINT ( 'NONE',  ( -45.52287095715006160, -29.50250786944525672, 11.44777988621624054 ) ) ;
#70387=DIRECTION ( 'NONE',  ( -3.773278334444166432E-23, 1.000000000000000000, 0.000000000000000000 ) ) ;
#70388=VERTEX_POINT ( 'NONE', #6240 ) ;
#70389=CARTESIAN_POINT ( 'NONE',  ( -92.62287095715005592, -24.64898659630368627, 1.056161002820827921 ) ) ;
#70390=FACE_OUTER_BOUND ( 'NONE', #12224, .T. ) ;
#70391=ORIENTED_EDGE ( 'NONE', *, *, #65306, .T. ) ;
#70392=EDGE_CURVE ( 'NONE', #54069, #60061, #98817, .T. ) ;
#70393=CARTESIAN_POINT ( 'NONE',  ( -16.05948562299510485, -12.68841425896798469, 11.49999999999998934 ) ) ;
#70395=EDGE_LOOP ( 'NONE', ( #82190, #46847, #74155, #57481 ) ) ;
#70396=ORIENTED_EDGE ( 'NONE', *, *, #28822, .T. ) ;
#70397=B_SPLINE_CURVE_WITH_KNOTS ( 'NONE', 3,
 ( #18473, #81375, #82366, #49444 ),
 .UNSPECIFIED., .F., .F.,
 ( 4, 4 ),
 ( 1.387778780781445676E-17, 0.0001000000000000028508 ),
 .UNSPECIFIED. ) ;
#70398=VERTEX_POINT ( 'NONE', #100060 ) ;
#70399=CARTESIAN_POINT ( 'NONE',  ( -13.16640216892762894, -18.94680327863774849, -1.500000000000002220 ) ) ;
#70400=CARTESIAN_POINT ( 'NONE',  ( -50.06200402506829761, -25.12646615760390034, 2.865550471351198336 ) ) ;
#70401=CARTESIAN_POINT ( 'NONE',  ( -20.27173212042777806, -0.06527795377243154895, -1.500000000000002220 ) ) ;
#70402=EDGE_CURVE ( 'NONE', #24545, #71288, #74738, .T. ) ;
#70403=EDGE_LOOP ( 'NONE', ( #6763, #17114, #47195, #91093 ) ) ;
#70405=CARTESIAN_POINT ( 'NONE',  ( -92.50697978749521155, -24.51314013834316796, 0.6176544820404240577 ) ) ;
#70406=EDGE_CURVE ( 'NONE', #67931, #93833, #49256, .T. ) ;
#70407=LINE ( 'NONE', #2913, #48104 ) ;
#70409=CARTESIAN_POINT ( 'NONE',  ( 14.19067371521932230, 16.14321034643037578, 11.49999999999999645 ) ) ;
#70410=ORIENTED_EDGE ( 'NONE', *, *, #27290, .T. ) ;
#70411=CARTESIAN_POINT ( 'NONE',  ( -75.57899749970765413, -25.00158670708910691, 2.256160236439223699 ) ) ;
#70413=EDGE_CURVE ( 'NONE', #31094, #55321, #99078, .T. ) ;
#70414=VECTOR ( 'NONE', #50382, 1000.000000000000114 ) ;
#70416=EDGE_CURVE ( 'NONE', #95213, #97694, #51766, .T. ) ;
#70417=CARTESIAN_POINT ( 'NONE',  ( 10.87737074370964407, 17.65887017642603851, -1.500000000000002220 ) ) ;
#70421=CARTESIAN_POINT ( 'NONE',  ( -41.64113801341388665, -24.15620529776627379, 10.23563542870660825 ) ) ;
#70422=CARTESIAN_POINT ( 'NONE',  ( -129.5895376238167387, -23.47596703998600631, 11.44779298504227683 ) ) ;
#70424=ORIENTED_EDGE ( 'NONE', *, *, #97294, .F. ) ;
#70426=DIRECTION ( 'NONE',  ( 0.000000000000000000, -2.173523156925979552E-06, 0.9999999999976378895 ) ) ;
#70427=EDGE_CURVE ( 'NONE', #27337, #884, #67390, .T. ) ;
#70428=CARTESIAN_POINT ( 'NONE',  ( -31.52287095715006160, -23.47593901973090169, -1.443836447538997536 ) ) ;
#70429=CARTESIAN_POINT ( 'NONE',  ( 2.959355296939036872, -21.81356824310248399, 11.49999999999999645 ) ) ;
#70431=CARTESIAN_POINT ( 'NONE',  ( -22.55165446212525993, 1.111233042438415808, -1.500000000000002220 ) ) ;
#70432=CARTESIAN_POINT ( 'NONE',  ( 14.09988904737591575, 15.55221489148801872, -1.500000000000002220 ) ) ;
#70435=VERTEX_POINT ( 'NONE', #45319 ) ;
#70437=CARTESIAN_POINT ( 'NONE',  ( -88.52287095715004739, -24.50321055353805377, 9.387540953477513384 ) ) ;
#70438=AXIS2_PLACEMENT_3D ( 'NONE', #19320, #34565, #9719 ) ;
#70439=B_SPLINE_CURVE_WITH_KNOTS ( 'NONE', 3,
 ( #52693, #45089, #29848, #60817 ),
 .UNSPECIFIED., .F., .F.,
 ( 4, 4 ),
 ( 0.000000000000000000, 9.999999999997510880E-05 ),
 .UNSPECIFIED. ) ;
#70442=CARTESIAN_POINT ( 'NONE',  ( 15.93590435955092843, -13.91358336426615239, -1.500000000000002220 ) ) ;
#70443=CARTESIAN_POINT ( 'NONE',  ( -82.62287095715007013, -24.34917612406837861, 0.1852690917426655925 ) ) ;
#70444=CARTESIAN_POINT ( 'NONE',  ( -51.63614490863932360, -25.03148624446666304, 7.022166193333077011 ) ) ;
#70445=CARTESIAN_POINT ( 'NONE',  ( -121.5205784047497275, -23.96119346886880308, -0.6495511937832032512 ) ) ;
#70446=LINE ( 'NONE', #24264, #5379 ) ;
#70448=CARTESIAN_POINT ( 'NONE',  ( -5.848988146064017180, 21.40304369876291446, -1.500000000000002220 ) ) ;
#70449=CARTESIAN_POINT ( 'NONE',  ( -81.55435809614610321, -23.96169478059713143, 10.65365249895718591 ) ) ;
#70450=EDGE_CURVE ( 'NONE', #41069, #76295, #4495, .T. ) ;
#70452=ORIENTED_EDGE ( 'NONE', *, *, #18605, .T. ) ;
#70453=CARTESIAN_POINT ( 'NONE',  ( -51.85051548866884019, -25.31633255200107158, 5.725680900099839654 ) ) ;
#70454=CARTESIAN_POINT ( 'NONE',  ( -60.62287095715004881, -29.50247984919015209, -1.443849546365056913 ) ) ;
#70455=CARTESIAN_POINT ( 'NONE',  ( -126.5902073896861282, -23.96119346886880663, -0.6495511937832031402 ) ) ;
#70456=EDGE_CURVE ( 'NONE', #53720, #46308, #6737, .T. ) ;
#70457=DIRECTION ( 'NONE',  ( -1.000000000000000000, -3.773278334444167608E-23, -8.201307833595939069E-29 ) ) ;
#70459=CARTESIAN_POINT ( 'NONE',  ( -3.206006181753352724, -19.19236486397402430, -1.500000000000002220 ) ) ;
#70460=CARTESIAN_POINT ( 'NONE',  ( 21.30238844577196389, 2.035401582669650544, 11.49999999999998934 ) ) ;
#70462=FACE_OUTER_BOUND ( 'NONE', #85872, .T. ) ;
#70464=CARTESIAN_POINT ( 'NONE',  ( -44.52287095715006870, -23.72773821059535848, 11.05748984161097326 ) ) ;
#70465=CARTESIAN_POINT ( 'NONE',  ( -12.60694655700363143, 18.86142483545513926, -1.500000000000002220 ) ) ;
#70466=EDGE_CURVE ( 'NONE', #25473, #37715, #44387, .T. ) ;
#70469=CARTESIAN_POINT ( 'NONE',  ( 19.84127317031322946, -0.4231496731191971561, 11.49999999999999645 ) ) ;
#70471=CARTESIAN_POINT ( 'NONE',  ( -73.62287095715009855, -23.94994826722515313, -0.6494450866351700880 ) ) ;
#70475=ADVANCED_FACE ( 'NONE', ( #61043 ), #91975, .T. ) ;
#70476=CARTESIAN_POINT ( 'NONE',  ( -30.47287095715007510, -23.47594215783195537, -5.102550391006585557E-05 ) ) ;
#70477=CARTESIAN_POINT ( 'NONE',  ( -74.52287095715004739, -24.66019654487200441, 8.947790411086112172 ) ) ;
#70478=CARTESIAN_POINT ( 'NONE',  ( -0.4625342273119020797, 21.68341340789531912, 11.49999999999998934 ) ) ;
#70479=CARTESIAN_POINT ( 'NONE',  ( -31.62287095715005236, -24.66019654487199020, 8.947790411086138818 ) ) ;
#70480=CARTESIAN_POINT ( 'NONE',  ( 19.46547125265945155, -1.073068822128883104, -1.500000000000002220 ) ) ;
#70481=B_SPLINE_CURVE_WITH_KNOTS ( 'NONE', 3,
 ( #77384, #61694, #60698, #14996, #38335, #37841 ),
 .UNSPECIFIED., .F., .F.,
 ( 4, 2, 4 ),
 ( 6.391158118952235087E-06, 0.001387004593080770317, 0.002767618028042588118 ),
 .UNSPECIFIED. ) ;
#70482=CARTESIAN_POINT ( 'NONE',  ( -123.6228709571501270, -24.35013146730204525, 9.818937971375101270 ) ) ;
#70484=B_SPLINE_CURVE_WITH_KNOTS ( 'NONE', 3,
 ( #76060, #15162, #30894, #68463, #53245, #6055 ),
 .UNSPECIFIED., .F., .F.,
 ( 4, 2, 4 ),
 ( 1.570755371633993761E-05, 0.001396183895866086669, 0.002776660238015833410 ),
 .UNSPECIFIED. ) ;
#70486=CARTESIAN_POINT ( 'NONE',  ( -20.29798418530817017, 1.744846428065259136, 11.49999999999999645 ) ) ;
#70487=CARTESIAN_POINT ( 'NONE',  ( -80.54344909021948240, -24.63355581998386157, 0.9682620441943954326 ) ) ;
#70490=ORIENTED_EDGE ( 'NONE', *, *, #18510, .T. ) ;
#70491=CARTESIAN_POINT ( 'NONE',  ( -0.06345841168740280758, -22.22848099251229570, 9.439037205594624780 ) ) ;
#70493=CARTESIAN_POINT ( 'NONE',  ( -49.20147844880023058, -25.31601899827206381, 5.321223608784601211 ) ) ;
#70496=CARTESIAN_POINT ( 'NONE',  ( 7.746586651691365510, 18.53313339873204058, 11.49999999999998934 ) ) ;
#70497=CARTESIAN_POINT ( 'NONE',  ( -109.5591676267192156, -23.48783264082476663, -1.443836473390089692 ) ) ;
#70500=CARTESIAN_POINT ( 'NONE',  ( -14.16064136294604303, -18.02537036913223290, 11.49999999999999645 ) ) ;
#70501=CARTESIAN_POINT ( 'NONE',  ( -20.46125754976198508, 9.905080999540670561, 11.49999999999998934 ) ) ;
#70503=CARTESIAN_POINT ( 'NONE',  ( -53.62287095715009855, -24.35013146730203459, 9.818937971375113705 ) ) ;
#70504=CARTESIAN_POINT ( 'NONE',  ( -28.52287095715004739, -24.18758155425416945, 0.1850819526199724008 ) ) ;
#70506=CARTESIAN_POINT ( 'NONE',  ( -30.57287095715007297, -24.05819166410570276, 10.46738261685066007 ) ) ;
#70509=CARTESIAN_POINT ( 'NONE',  ( -98.89396085167129513, -25.31200736282745112, 6.074556455972243363 ) ) ;
#70510=ORIENTED_EDGE ( 'NONE', *, *, #85401, .F. ) ;
#70511=CARTESIAN_POINT ( 'NONE',  ( -19.36681041099238598, 6.328833669845586485, 11.49999999999998934 ) ) ;
#70513=EDGE_CURVE ( 'NONE', #52940, #85301, #63827, .T. ) ;
#70514=CARTESIAN_POINT ( 'NONE',  ( -16.20615075098634961, 16.30094363606528418, -1.500000000000002220 ) ) ;
#70518=VERTEX_POINT ( 'NONE', #63557 ) ;
#70521=CARTESIAN_POINT ( 'NONE',  ( -53.49127501850180977, -24.51419770103157347, 9.386484678747180510 ) ) ;
#70522=CARTESIAN_POINT ( 'NONE',  ( 21.27783752795556538, -0.9766432368044721812, 11.49999999999999645 ) ) ;
#70523=EDGE_LOOP ( 'NONE', ( #14161, #2029, #38944, #42877 ) ) ;
#70524=EDGE_CURVE ( 'NONE', #13524, #40340, #22612, .T. ) ;
#70525=ORIENTED_EDGE ( 'NONE', *, *, #59185, .F. ) ;
#70526=CARTESIAN_POINT ( 'NONE',  ( -21.61287440533560300, 5.199345243644041936, -1.500000000000002220 ) ) ;
#70527=EDGE_CURVE ( 'NONE', #84975, #32236, #14178, .T. ) ;
#70528=CARTESIAN_POINT ( 'NONE',  ( 19.88596897151998633, -5.565664080715476913, 11.49999999999998934 ) ) ;
#70529=ORIENTED_EDGE ( 'NONE', *, *, #99608, .F. ) ;
#70530=CARTESIAN_POINT ( 'NONE',  ( -109.3320997930167806, -25.31627335646685495, 5.169840710465035905 ) ) ;
#70531=CARTESIAN_POINT ( 'NONE',  ( -95.50968202525180573, -24.40133493613050319, 9.663955038902802386 ) ) ;
#70532=ORIENTED_EDGE ( 'NONE', *, *, #81448, .T. ) ;
#70533=PLANE ( 'NONE',  #36468 ) ;
#70534=ORIENTED_EDGE ( 'NONE', *, *, #60336, .F. ) ;
#70535=CARTESIAN_POINT ( 'NONE',  ( -58.48920519830264908, -24.66019654487199730, 8.947790411086117501 ) ) ;
#70536=CARTESIAN_POINT ( 'NONE',  ( -48.52287095715008292, -23.94994826722564341, -0.6494450866342713624 ) ) ;
#70537=CARTESIAN_POINT ( 'NONE',  ( -20.64841573231975147, 3.066018724555340746, -1.500000000000002220 ) ) ;
#70538=EDGE_CURVE ( 'NONE', #28046, #51976, #73497, .T. ) ;
#70539=CARTESIAN_POINT ( 'NONE',  ( -5.042499505632127565, 21.24692939306837758, 11.49999999999999645 ) ) ;
#70540=CARTESIAN_POINT ( 'NONE',  ( -26.92109862195654202, -24.89279950334402614, 7.359061847596003680 ) ) ;
#70542=CARTESIAN_POINT ( 'NONE',  ( 18.89768980500364037, -12.13386209897132773, -1.500000000000002220 ) ) ;
#70543=CARTESIAN_POINT ( 'NONE',  ( -118.5555930860171401, -23.96169478059713853, 10.65365249895717348 ) ) ;
#70544=CARTESIAN_POINT ( 'NONE',  ( -58.52287095715008292, -24.51283580621365132, 0.6167428607019717068 ) ) ;
#70547=ORIENTED_EDGE ( 'NONE', *, *, #79097, .F. ) ;
#70550=CARTESIAN_POINT ( 'NONE',  ( 12.49974722350246736, 17.29906535522423638, -1.500000000000002220 ) ) ;
#70551=CARTESIAN_POINT ( 'NONE',  ( 6.497064355747536268, 21.42967291005575348, 11.49999999999999645 ) ) ;
#70553=CARTESIAN_POINT ( 'NONE',  ( -16.48755246578841849, -13.11705038010048163, -1.500000000000002220 ) ) ;
#70554=CARTESIAN_POINT ( 'NONE',  ( -30.62471892381331529, -24.05745470861603152, -0.4713115009884515927 ) ) ;
#70555=CARTESIAN_POINT ( 'NONE',  ( -14.87316555497233495, -13.31901947624662519, -1.500000000000002220 ) ) ;
#70558=CARTESIAN_POINT ( 'NONE',  ( -20.77788740438921522, -7.151594987469691134, -1.500000000000002220 ) ) ;
#70562=CARTESIAN_POINT ( 'NONE',  ( -70.58953762381672448, -23.47593901973091235, -1.443836447539006196 ) ) ;
#70563=CARTESIAN_POINT ( 'NONE',  ( 19.25983760003161294, 7.974354923662064998, 11.49999999999999645 ) ) ;
#70564=EDGE_CURVE ( 'NONE', #68398, #15801, #32576, .T. ) ;
#70566=B_SPLINE_CURVE_WITH_KNOTS ( 'NONE', 3,
 ( #91032, #19520, #13401, #83413 ),
 .UNSPECIFIED., .F., .F.,
 ( 4, 4 ),
 ( 0.8411006093570028153, 0.8501070406291183490 ),
 .UNSPECIFIED. ) ;
#70567=DIRECTION ( 'NONE',  ( -0.000000000000000000, 2.173523156925979552E-06, -0.9999999999976378895 ) ) ;
#70569=CARTESIAN_POINT ( 'NONE',  ( 0.2649960030224881025, 21.33594185153759426, 11.49999999999998934 ) ) ;
#70571=CARTESIAN_POINT ( 'NONE',  ( -117.5228709571501184, -23.96177878511310055, 10.65340807706329684 ) ) ;
#70574=CARTESIAN_POINT ( 'NONE',  ( -125.6228709571500559, -29.50247984919015209, -1.443849546365044922 ) ) ;
#70575=DIRECTION ( 'NONE',  ( -3.773278334453079618E-23, 0.9999999999976377785, 2.173523156925978705E-06 ) ) ;
#70576=CARTESIAN_POINT ( 'NONE',  ( -11.40494320173684351, 19.43794304404440254, -1.500000000000002220 ) ) ;
#70578=VECTOR ( 'NONE', #21443, 1000.000000000000114 ) ;
#70583=CARTESIAN_POINT ( 'NONE',  ( 18.75866648459458830, -6.009157199652424453, 11.49999999999999645 ) ) ;
#70586=CARTESIAN_POINT ( 'NONE',  ( -120.6228709571500417, -29.50248528299804818, 1.056150453629045360 ) ) ;
#70587=ORIENTED_EDGE ( 'NONE', *, *, #20566, .F. ) ;
#70589=CARTESIAN_POINT ( 'NONE',  ( -99.55496185298399325, -23.96119346886881374, -0.6495511937831867089 ) ) ;
#70591=CARTESIAN_POINT ( 'NONE',  ( -61.52287095715009002, -23.73934037231757088, 11.05740245334329153 ) ) ;
#70592=CARTESIAN_POINT ( 'NONE',  ( -9.607006924060957687, -21.85068815744421045, 11.44779298504228038 ) ) ;
#70593=CARTESIAN_POINT ( 'NONE',  ( 9.261118129494249729, -17.44851725036260248, -1.500000000000002220 ) ) ;
#70594=ORIENTED_EDGE ( 'NONE', *, *, #83211, .T. ) ;
#70595=CARTESIAN_POINT ( 'NONE',  ( -109.4872011792213442, -25.24971315249232262, 3.733106366897268380 ) ) ;
#70599=ORIENTED_EDGE ( 'NONE', *, *, #1144, .T. ) ;
#70602=CARTESIAN_POINT ( 'NONE',  ( -100.5551968661962832, -25.30262289663432185, 4.733994061935349329 ) ) ;
#70603=CARTESIAN_POINT ( 'NONE',  ( -98.89534031563961491, -25.26638239608887915, 6.173962649882215104 ) ) ;
#70604=CARTESIAN_POINT ( 'NONE',  ( -67.62287095715005592, -23.47593901973091235, -1.443836447539006196 ) ) ;
#70605=CARTESIAN_POINT ( 'NONE',  ( -89.81226385320381667, -25.26877915520014994, 5.947789088310639904 ) ) ;
#70606=CARTESIAN_POINT ( 'NONE',  ( -86.62287095715005592, -23.48786465467241413, 11.44779295918254469 ) ) ;
#70607=CARTESIAN_POINT ( 'NONE',  ( -3.121018476474317183, -19.76494895549465980, 11.49999999999998934 ) ) ;
#70608=CARTESIAN_POINT ( 'NONE',  ( -58.62287095715004881, -23.47593901973091235, -1.443836447539007972 ) ) ;
#70609=CARTESIAN_POINT ( 'NONE',  ( -116.6242992002620440, -24.51419770103160189, 9.386484678747169852 ) ) ;
#70610=VERTEX_POINT ( 'NONE', #23957 ) ;
#70611=EDGE_CURVE ( 'NONE', #66746, #90746, #62525, .T. ) ;
#70612=ADVANCED_FACE ( 'NONE', ( #78730 ), #1136, .F. ) ;
#70613=CARTESIAN_POINT ( 'NONE',  ( -79.51271330033607398, -23.96169478059713143, 10.65365249895718058 ) ) ;
#70615=CARTESIAN_POINT ( 'NONE',  ( -109.6405337342305302, -25.18430212153996095, 3.562353486846156603 ) ) ;
#70616=CARTESIAN_POINT ( 'NONE',  ( -35.54076835017719560, -24.40034930558991277, 0.3402023900116170063 ) ) ;
#70620=B_SPLINE_CURVE_WITH_KNOTS ( 'NONE', 3,
 ( #78122, #66692, #97603, #89998, #80146, #3036 ),
 .UNSPECIFIED., .F., .F.,
 ( 4, 2, 4 ),
 ( 0.000000000000000000, 0.001380901958385387894, 0.002761803916770775788 ),
 .UNSPECIFIED. ) ;
#70621=CARTESIAN_POINT ( 'NONE',  ( -62.62287095715004881, -23.48786465467241058, 11.44779295918254824 ) ) ;
#70622=CARTESIAN_POINT ( 'NONE',  ( -73.62287095715007013, -23.96127896941632685, -0.6493128931037860374 ) ) ;
#70624=CARTESIAN_POINT ( 'NONE',  ( 14.62039552936377085, -14.08751720214925207, -1.500000000000002220 ) ) ;
#70625=EDGE_CURVE ( 'NONE', #73156, #11909, #91637, .T. ) ;
#70627=DIRECTION ( 'NONE',  ( 1.000000000000000000, 3.773278334444166432E-23, 8.201307841325785021E-29 ) ) ;
#70628=ORIENTED_EDGE ( 'NONE', *, *, #67200, .F. ) ;
#70629=CARTESIAN_POINT ( 'NONE',  ( -32.99388727629348494, -25.12026506542017046, 2.831122744435439209 ) ) ;
#70630=CARTESIAN_POINT ( 'NONE',  ( -17.16780662754360520, -10.58209718439171176, -1.500000000000002220 ) ) ;
#70631=CARTESIAN_POINT ( 'NONE',  ( 17.61891135320703938, 11.69080507458975227, 11.49999999999999645 ) ) ;
#70632=CARTESIAN_POINT ( 'NONE',  ( 14.84500176111689207, -16.38379996218902335, -1.500000000000002220 ) ) ;
#70633=EDGE_CURVE ( 'NONE', #2140, #41031, #83191, .T. ) ;
#70634=CARTESIAN_POINT ( 'NONE',  ( 18.81462172601333549, -8.267562025728075525, 11.49999999999998934 ) ) ;
#70635=AXIS2_PLACEMENT_3D ( 'NONE', #4497, #59271, #43552 ) ;
#70639=VERTEX_POINT ( 'NONE', #1642 ) ;
#70640=EDGE_CURVE ( 'NONE', #25509, #96582, #64063, .T. ) ;
#70641=DIRECTION ( 'NONE',  ( -3.773278334444166432E-23, 1.000000000000000000, 0.000000000000000000 ) ) ;
#70642=CARTESIAN_POINT ( 'NONE',  ( -86.22287095715006444, -23.47593901973090169, -1.443836447538996870 ) ) ;
#70643=ORIENTED_EDGE ( 'NONE', *, *, #31698, .F. ) ;
#70645=ORIENTED_EDGE ( 'NONE', *, *, #19983, .F. ) ;
#70647=ORIENTED_EDGE ( 'NONE', *, *, #49112, .F. ) ;
#70648=CARTESIAN_POINT ( 'NONE',  ( -110.9760276224984779, -25.14607537338261523, 2.978229960058158099 ) ) ;
#70650=CARTESIAN_POINT ( 'NONE',  ( -68.63577537931014660, -24.15620529776627734, 10.23563542870660825 ) ) ;
#70651=CARTESIAN_POINT ( 'NONE',  ( -4.528870947376731237, 20.18191347215651987, -1.500000000000002220 ) ) ;
#70654=CARTESIAN_POINT ( 'NONE',  ( 18.46943957830784555, -11.30625484363265265, 11.49999999999999645 ) ) ;
#70658=CARTESIAN_POINT ( 'NONE',  ( -1.374798071107336206, -22.32369649477951512, -1.500000000000002220 ) ) ;
#70660=EDGE_CURVE ( 'NONE', #25743, #20125, #60219, .T. ) ;
#70661=CARTESIAN_POINT ( 'NONE',  ( -47.53537244378864557, -24.51419770103156637, 9.386484678747176957 ) ) ;
#70662=CARTESIAN_POINT ( 'NONE',  ( -101.5228709571500332, -23.95044443724991723, 10.65354141964649237 ) ) ;
#70663=ORIENTED_EDGE ( 'NONE', *, *, #2132, .F. ) ;
#70664=CARTESIAN_POINT ( 'NONE',  ( -119.2832211118485333, -25.38369257465123496, 5.756917303100165029 ) ) ;
#70665=CARTESIAN_POINT ( 'NONE',  ( -52.55620429048339304, -24.64965694238575011, 8.947790433994201820 ) ) ;
#70666=EDGE_LOOP ( 'NONE', ( #19256, #78281, #45834, #51817 ) ) ;
#70667=CARTESIAN_POINT ( 'NONE',  ( -45.52287095715006160, -24.82576562948885623, 8.398263436605494903 ) ) ;
#70669=FACE_OUTER_BOUND ( 'NONE', #34160, .T. ) ;
#70670=CARTESIAN_POINT ( 'NONE',  ( -10.65520286329281596, -18.28862552182625123, -1.500000000000002220 ) ) ;
#70671=ORIENTED_EDGE ( 'NONE', *, *, #32701, .T. ) ;
#70672=CARTESIAN_POINT ( 'NONE',  ( -50.55080355490176203, -24.15503026093912808, -0.2815557561904566963 ) ) ;
#70673=CARTESIAN_POINT ( 'NONE',  ( -21.69466673205137752, 2.402554924997643226, -1.500000000000002220 ) ) ;
#70676=CARTESIAN_POINT ( 'NONE',  ( -109.5562042904833788, -24.65952944569305316, 1.056160979905704345 ) ) ;
#70677=CARTESIAN_POINT ( 'NONE',  ( -21.01659442711627790, -5.882202039844940167, -1.500000000000002220 ) ) ;
#70680=CARTESIAN_POINT ( 'NONE',  ( -41.62287095715006302, -23.47593901973091235, -1.443836447539011525 ) ) ;
#70681=CARTESIAN_POINT ( 'NONE',  ( -51.62287095715005592, -23.48783264082478084, -1.443836473390070596 ) ) ;
#70685=EDGE_CURVE ( 'NONE', #30482, #59154, #58924, .T. ) ;
#70686=EDGE_LOOP ( 'NONE', ( #83054, #8986, #24707, #91389 ) ) ;
#70688=FACE_OUTER_BOUND ( 'NONE', #72065, .T. ) ;
#70689=CARTESIAN_POINT ( 'NONE',  ( 3.248270302591931724, 20.98854991013365279, -1.500000000000002220 ) ) ;
#70690=CARTESIAN_POINT ( 'NONE',  ( -121.6228709571500417, -24.50216790748098816, 0.6166512839513769162 ) ) ;
#70691=CARTESIAN_POINT ( 'NONE',  ( -130.5728709571500588, -24.57438384523504027, 0.5319095616429418971 ) ) ;
#70694=CARTESIAN_POINT ( 'NONE',  ( 15.46825748771582631, 11.69065726450791409, -1.500000000000002220 ) ) ;
#70696=CARTESIAN_POINT ( 'NONE',  ( -40.94210688951491051, -25.03707806782366418, 7.590868867492675420 ) ) ;
#70697=ORIENTED_EDGE ( 'NONE', *, *, #62263, .T. ) ;
#70698=B_SPLINE_CURVE_WITH_KNOTS ( 'NONE', 3,
 ( #8440, #78437, #76433, #8938 ),
 .UNSPECIFIED., .F., .F.,
 ( 4, 4 ),
 ( 0.000000000000000000, 0.0001000000000000167422 ),
 .UNSPECIFIED. ) ;
#70699=CARTESIAN_POINT ( 'NONE',  ( -16.16875682573952133, 10.94412424577950915, 11.49999999999999645 ) ) ;
#70700=CARTESIAN_POINT ( 'NONE',  ( -42.52287095715007581, -24.33927499327854349, 9.819080762295817166 ) ) ;
#70701=CARTESIAN_POINT ( 'NONE',  ( -68.52287095715004739, -24.50216790748206463, 0.6166512839542471758 ) ) ;
#70702=ORIENTED_EDGE ( 'NONE', *, *, #18038, .F. ) ;
#70703=B_SPLINE_CURVE_WITH_KNOTS ( 'NONE', 3,
 ( #69707, #76297, #30129, #30632 ),
 .UNSPECIFIED., .F., .F.,
 ( 4, 4 ),
 ( 0.2206575661668280786, 0.2296639974389436401 ),
 .UNSPECIFIED. ) ;
#70704=CARTESIAN_POINT ( 'NONE',  ( -93.62287095715005592, -24.64898659630367916, 1.056161002820827921 ) ) ;
#70705=PLANE ( 'NONE',  #85449 ) ;
#70708=CARTESIAN_POINT ( 'NONE',  ( -93.63682493047612354, -23.73791477778911840, 11.05961554403170410 ) ) ;
#70709=CARTESIAN_POINT ( 'NONE',  ( -15.16444148636751521, -12.51942901160708921, 11.49999999999998934 ) ) ;
#70710=CARTESIAN_POINT ( 'NONE',  ( -41.08147698621603894, -25.31583728001788103, 4.883364621082173507 ) ) ;
#70711=ORIENTED_EDGE ( 'NONE', *, *, #39788, .F. ) ;
#70712=CARTESIAN_POINT ( 'NONE',  ( 21.54666897473465070, 1.519730039111064412, 11.49999999999998934 ) ) ;
#70713=DIRECTION ( 'NONE',  ( -3.773278334453080206E-23, 0.9999999999976377785, 2.173523156925979975E-06 ) ) ;
#70715=CARTESIAN_POINT ( 'NONE',  ( 1.702247502073919394, 23.03039350466679025, -1.500000000000002220 ) ) ;
#70716=ADVANCED_FACE ( 'NONE', ( #34092 ), #74634, .F. ) ;
#70718=CARTESIAN_POINT ( 'NONE',  ( -92.52287095715006160, -23.47593901973090169, -1.443836447538996426 ) ) ;
#70719=PLANE ( 'NONE',  #65279 ) ;
#70721=CARTESIAN_POINT ( 'NONE',  ( -104.5228709571500190, -23.95044443724992078, 10.65354141964649415 ) ) ;
#70723=AXIS2_PLACEMENT_3D ( 'NONE', #56089, #36977, #84141 ) ;
#70724=CARTESIAN_POINT ( 'NONE',  ( -111.6658724870577117, -25.10921570101833211, 3.734856220746116673 ) ) ;
#70725=FACE_OUTER_BOUND ( 'NONE', #76441, .T. ) ;
#70726=CARTESIAN_POINT ( 'NONE',  ( -99.12380231474227799, -25.31565897376004415, 4.001575044103979018 ) ) ;
#70727=CARTESIAN_POINT ( 'NONE',  ( 2.927915493035635031, 19.71835975189664936, 11.49999999999998934 ) ) ;
#70728=CARTESIAN_POINT ( 'NONE',  ( -75.54715773856550243, -24.40133493613049964, 9.663955038902805939 ) ) ;
#70729=ADVANCED_FACE ( 'NONE', ( #88372 ), #43696, .T. ) ;
#70730=CARTESIAN_POINT ( 'NONE',  ( 1.158388978951967463, 19.79969207489630634, -1.500000000000002220 ) ) ;
#70731=EDGE_LOOP ( 'NONE', ( #51697, #98484, #87902, #31213 ) ) ;
#70732=EDGE_CURVE ( 'NONE', #10916, #29962, #57941, .T. ) ;
#70734=CARTESIAN_POINT ( 'NONE',  ( -56.51486553911006183, -23.73766607897670511, -1.055555164236459342 ) ) ;
#70736=EDGE_CURVE ( 'NONE', #39701, #73698, #54103, .T. ) ;
#70738=LINE ( 'NONE', #32667, #44313 ) ;
#70739=CARTESIAN_POINT ( 'NONE',  ( -20.55201672899488585, 2.666056886502145673, 11.49999999999999645 ) ) ;
#70740=CARTESIAN_POINT ( 'NONE',  ( -86.52287095715006160, -24.65952944569304606, 1.056160979905700570 ) ) ;
#70741=CARTESIAN_POINT ( 'NONE',  ( -88.62287095715005592, -24.33832256526968862, 0.1851278514119913954 ) ) ;
#70742=CARTESIAN_POINT ( 'NONE',  ( 7.803535043518188274, -21.38454823780343617, 11.49999999999999645 ) ) ;
#70745=CARTESIAN_POINT ( 'NONE',  ( -70.07901916590789426, -25.12717508165702895, 7.077626925157802340 ) ) ;
#70746=ORIENTED_EDGE ( 'NONE', *, *, #75795, .T. ) ;
#70747=CARTESIAN_POINT ( 'NONE',  ( -17.27845874757997535, -10.49745931960568335, 11.49999999999998934 ) ) ;
#70748=EDGE_CURVE ( 'NONE', #33585, #53678, #80681, .T. ) ;
#70749=EDGE_CURVE ( 'NONE', #98717, #34234, #27499, .T. ) ;
#70751=CARTESIAN_POINT ( 'NONE',  ( -97.62287095715004170, -24.50321055353806088, 9.387540953477529371 ) ) ;
#70754=CARTESIAN_POINT ( 'NONE',  ( -8.048360580058307789, -21.46040670285860230, -1.500000000000002220 ) ) ;
#70755=CARTESIAN_POINT ( 'NONE',  ( -50.75699389676201889, -25.18439660648728307, 3.343798628745027202 ) ) ;
#70756=CARTESIAN_POINT ( 'NONE',  ( 10.17626895549074817, -17.22257424524772418, -1.500000000000002220 ) ) ;
#70758=CARTESIAN_POINT ( 'NONE',  ( 11.32296221242833667, -17.63459971646239310, 11.49999999999999645 ) ) ;
#70763=CARTESIAN_POINT ( 'NONE',  ( -21.70078857174656761, -3.768841730229552045, -1.500000000000002220 ) ) ;
#70764=EDGE_CURVE ( 'NONE', #67184, #86369, #42713, .T. ) ;
#70767=CARTESIAN_POINT ( 'NONE',  ( -49.79812375574695693, -25.18440137848927307, 3.459241766176638144 ) ) ;
#70768=CARTESIAN_POINT ( 'NONE',  ( -43.52287095715006160, -23.48786465467240347, 11.44779295918255180 ) ) ;
#70769=ORIENTED_EDGE ( 'NONE', *, *, #16911, .F. ) ;
#70771=EDGE_LOOP ( 'NONE', ( #4556, #54424, #8419, #3987 ) ) ;
#70773=CARTESIAN_POINT ( 'NONE',  ( -101.5084176993576648, -25.26303730729093644, 3.986250639247583827 ) ) ;
#70774=CARTESIAN_POINT ( 'NONE',  ( -101.0021142486707646, -25.10935827596331649, 2.948027515349565419 ) ) ;
#70776=CARTESIAN_POINT ( 'NONE',  ( 1.945971545120378288, -20.36639758168144709, -1.500000000000002220 ) ) ;
#70777=ADVANCED_FACE ( 'NONE', ( #20336 ), #51308, .F. ) ;
#70778=ORIENTED_EDGE ( 'NONE', *, *, #19087, .F. ) ;
#70779=CARTESIAN_POINT ( 'NONE',  ( -79.52287095715006160, -24.50216790748204687, 0.6166512839542530600 ) ) ;
#70780=FACE_OUTER_BOUND ( 'NONE', #76725, .T. ) ;
#70782=CARTESIAN_POINT ( 'NONE',  ( 22.20884612314100792, -2.053178116692622623, 11.49999999999998934 ) ) ;
#70785=CARTESIAN_POINT ( 'NONE',  ( -32.62287095715004881, -24.64965695001467694, 8.947790433994189385 ) ) ;
#70786=PLANE ( 'NONE',  #82031 ) ;
#70788=EDGE_CURVE ( 'NONE', #37472, #72942, #17589, .T. ) ;
#70789=CARTESIAN_POINT ( 'NONE',  ( -29.76961320961419588, -25.20477499778818498, 4.020760705257079515 ) ) ;
#70790=B_SPLINE_CURVE_WITH_KNOTS ( 'NONE', 3,
 ( #52724, #45121, #76040, #53230 ),
 .UNSPECIFIED., .F., .F.,
 ( 4, 4 ),
 ( 0.1098643759392575470, 0.1188708072113730391 ),
 .UNSPECIFIED. ) ;
#70791=FACE_OUTER_BOUND ( 'NONE', #38818, .T. ) ;
#70792=CARTESIAN_POINT ( 'NONE',  ( -10.15938669249390180, 18.18672505111813464, -1.500000000000002220 ) ) ;
#70794=CARTESIAN_POINT ( 'NONE',  ( -52.52287095715006870, -24.65952944569303895, 1.056160979905693686 ) ) ;
#70798=CARTESIAN_POINT ( 'NONE',  ( -118.6228709571500701, -23.47596703998600631, 11.44779298504227683 ) ) ;
#70800=CARTESIAN_POINT ( 'NONE',  ( -19.96636262075925927, 6.592627302904066511, -1.500000000000002220 ) ) ;
#70801=ORIENTED_EDGE ( 'NONE', *, *, #70625, .T. ) ;
#70802=VECTOR ( 'NONE', #91136, 1000.000000000000114 ) ;
#70803=CARTESIAN_POINT ( 'NONE',  ( -118.5228709571500474, -23.95044443724993144, 10.65354141964648882 ) ) ;
#70806=AXIS2_PLACEMENT_3D ( 'NONE', #32103, #61077, #24491 ) ;
#70807=CARTESIAN_POINT ( 'NONE',  ( -86.54256729674141013, -24.66019654487200086, 8.947790411086117501 ) ) ;
#70808=DIRECTION ( 'NONE',  ( 1.000000000000000000, 3.773278334444166432E-23, 8.201307841325785021E-29 ) ) ;
#70810=CARTESIAN_POINT ( 'NONE',  ( -20.56814720681451902, 8.302189128749821734, 11.49999999999999645 ) ) ;
#70811=ORIENTED_EDGE ( 'NONE', *, *, #77135, .T. ) ;
#70813=CARTESIAN_POINT ( 'NONE',  ( -90.30662536647538730, -25.32594422361629327, 4.020877017707874757 ) ) ;
#70815=CARTESIAN_POINT ( 'NONE',  ( -21.72567761722203628, 6.514095075961352954, 11.49999999999998934 ) ) ;
#70817=CARTESIAN_POINT ( 'NONE',  ( -76.62287095715005592, -23.94994826722514958, -0.6494450866351715312 ) ) ;
#70819=EDGE_LOOP ( 'NONE', ( #7782, #69895, #87675, #32594 ) ) ;
#70821=CARTESIAN_POINT ( 'NONE',  ( 17.50376878386636292, -9.983289808088789741, 11.49999999999998934 ) ) ;
#70822=CARTESIAN_POINT ( 'NONE',  ( -80.62287095715007013, -24.52232992886361984, 0.6492154411906119194 ) ) ;
#70823=ORIENTED_EDGE ( 'NONE', *, *, #78088, .F. ) ;
#70824=DIRECTION ( 'NONE',  ( -3.773278334453080206E-23, 0.9999999999976377785, 2.173523156925979975E-06 ) ) ;
#70825=CARTESIAN_POINT ( 'NONE',  ( -17.72129891523481149, -13.73837202384828515, -1.500000000000002220 ) ) ;
#70826=B_SPLINE_CURVE_WITH_KNOTS ( 'NONE', 3,
 ( #62776, #23168, #78462, #54158 ),
 .UNSPECIFIED., .F., .F.,
 ( 4, 4 ),
 ( 0.5291485173198170466, 0.5301492643605828503 ),
 .UNSPECIFIED. ) ;
#70829=LINE ( 'NONE', #42886, #33626 ) ;
#70830=CARTESIAN_POINT ( 'NONE',  ( -94.63061136128430917, -24.15620529776628089, 10.23563542870660470 ) ) ;
#70831=CARTESIAN_POINT ( 'NONE',  ( -115.5228709571500616, -24.99156044556202616, 7.747789690856173195 ) ) ;
#70833=CARTESIAN_POINT ( 'NONE',  ( -106.5228709571500758, -29.50248528299804818, 1.056150453629043584 ) ) ;
#70834=FACE_BOUND ( 'NONE', #52795, .T. ) ;
#70835=CARTESIAN_POINT ( 'NONE',  ( -12.82114019720147802, -14.77593736753402709, -1.500000000000002220 ) ) ;
#70836=PLANE ( 'NONE',  #96009 ) ;
#70837=VERTEX_POINT ( 'NONE', #22331 ) ;
#70838=CARTESIAN_POINT ( 'NONE',  ( 7.367719877546908158, -20.20905560389912026, 11.49999999999998934 ) ) ;
#70840=CARTESIAN_POINT ( 'NONE',  ( -128.6238584515385242, -24.15543982623908548, -0.2315651400026392803 ) ) ;
#70841=CARTESIAN_POINT ( 'NONE',  ( -54.62287095715004170, -23.47596703998600631, 11.44779298504227505 ) ) ;
#70842=CARTESIAN_POINT ( 'NONE',  ( -113.5228709571500758, -23.96177878511310055, 10.65340807706329151 ) ) ;
#70844=CARTESIAN_POINT ( 'NONE',  ( 21.75294195941402364, -7.338126679257295670, -1.500000000000002220 ) ) ;
#70845=EDGE_CURVE ( 'NONE', #52051, #76238, #37003, .T. ) ;
#70847=PLANE ( 'NONE',  #19132 ) ;
#70848=CARTESIAN_POINT ( 'NONE',  ( -71.27691565640060389, -25.27723027174688042, 5.969665484188881877 ) ) ;
#70849=CARTESIAN_POINT ( 'NONE',  ( -3.121018476474317183, -19.76494895549465980, 11.49999999999999645 ) ) ;
#70850=CARTESIAN_POINT ( 'NONE',  ( -78.94637683104262749, -25.26612659742505329, 5.821637768010305081 ) ) ;
#70852=EDGE_CURVE ( 'NONE', #38855, #89848, #69717, .T. ) ;
#70853=EDGE_CURVE ( 'NONE', #32034, #61298, #84260, .T. ) ;
#70858=EDGE_CURVE ( 'NONE', #33481, #37811, #50308, .T. ) ;
#70859=CARTESIAN_POINT ( 'NONE',  ( 15.29254711327534899, -15.47666941828629739, -1.500000000000002220 ) ) ;
#70860=DIRECTION ( 'NONE',  ( -1.000000000000000000, -3.773278334444166432E-23, -8.201307841325785021E-29 ) ) ;
#70861=CARTESIAN_POINT ( 'NONE',  ( 9.421224358276909072, -17.24829524558457194, -1.500000000000002220 ) ) ;
#70862=ADVANCED_FACE ( 'NONE', ( #32466 ), #58772, .T. ) ;
#70864=CARTESIAN_POINT ( 'NONE',  ( -122.6228709571500559, -24.65952944569305316, 1.056160979905706343 ) ) ;
#70868=CARTESIAN_POINT ( 'NONE',  ( -38.52287095715006870, -23.47596703998600631, 11.44779298504229281 ) ) ;
#70870=CARTESIAN_POINT ( 'NONE',  ( -20.44794078217315558, 2.270689272194197805, 11.49999999999999645 ) ) ;
#70872=VECTOR ( 'NONE', #89979, 1000.000000000000114 ) ;
#70873=CARTESIAN_POINT ( 'NONE',  ( -120.5892038963322079, -24.63355581998386157, 0.9682620441943888823 ) ) ;
#70874=CARTESIAN_POINT ( 'NONE',  ( -21.91535228782390732, -5.629186751109307885, 11.49999999999999645 ) ) ;
#70876=CARTESIAN_POINT ( 'NONE',  ( -80.64675904551154417, -25.21083105912962807, 3.409327675794629808 ) ) ;
#70877=DIRECTION ( 'NONE',  ( -3.773278334453079618E-23, 0.9999999999976377785, 2.173523156925979975E-06 ) ) ;
#70878=CARTESIAN_POINT ( 'NONE',  ( -74.52287095715006160, -24.33927499327854349, 9.819080762295802955 ) ) ;
#70880=AXIS2_PLACEMENT_3D ( 'NONE', #49123, #20021, #78532 ) ;
#70881=ADVANCED_FACE ( 'NONE', ( #32976, #31968 ), #97659, .T. ) ;
#70882=CARTESIAN_POINT ( 'NONE',  ( -25.96779814532654385, -24.93063398007822684, 7.161765927771289064 ) ) ;
#70883=DIRECTION ( 'NONE',  ( -3.773278334444166432E-23, 1.000000000000000000, 0.000000000000000000 ) ) ;
#70886=CARTESIAN_POINT ( 'NONE',  ( -79.34687923781920915, -25.26750092165967132, 5.960409283396633562 ) ) ;
#70887=CARTESIAN_POINT ( 'NONE',  ( 7.824713763024562674, 21.46283361357968289, 11.49999999999998934 ) ) ;
#70888=CARTESIAN_POINT ( 'NONE',  ( -104.5228709571501184, -23.94994826722565762, -0.6494450866342743600 ) ) ;
#70889=CARTESIAN_POINT ( 'NONE',  ( -96.59382161140817402, -23.96119346886881019, -0.6495511937832062488 ) ) ;
#70890=CARTESIAN_POINT ( 'NONE',  ( -63.53555138627451981, -24.66019654487200086, 8.947790411086119278 ) ) ;
#70891=CARTESIAN_POINT ( 'NONE',  ( 15.63351008929417318, -16.12541905121107177, 11.49999999999999645 ) ) ;
#70892=ORIENTED_EDGE ( 'NONE', *, *, #88853, .T. ) ;
#70893=CARTESIAN_POINT ( 'NONE',  ( -34.62287095715006302, -23.72773821059535493, 11.05748984161097681 ) ) ;
#70894=CARTESIAN_POINT ( 'NONE',  ( -21.90371867972833542, 1.011951690471867060, -1.500000000000002220 ) ) ;
#70896=CARTESIAN_POINT ( 'NONE',  ( -44.54009632154533449, -24.35071581493543036, 9.817618358456025263 ) ) ;
#70897=CARTESIAN_POINT ( 'NONE',  ( -69.11640284054173833, -25.15929664862683879, 6.884326848992852632 ) ) ;
#70898=ORIENTED_EDGE ( 'NONE', *, *, #55967, .T. ) ;
#70899=CARTESIAN_POINT ( 'NONE',  ( -48.60674490981843121, -23.73791477778911840, 11.05961554403170766 ) ) ;
#70900=CARTESIAN_POINT ( 'NONE',  ( -89.40841769935767047, -29.50249591506787894, 5.947779886229223045 ) ) ;
#70902=CARTESIAN_POINT ( 'NONE',  ( -20.16212974941129588, 3.559051167911782887, 11.49999999999998934 ) ) ;
#70903=ORIENTED_EDGE ( 'NONE', *, *, #49631, .F. ) ;
#70906=ORIENTED_EDGE ( 'NONE', *, *, #81323, .T. ) ;
#70907=CARTESIAN_POINT ( 'NONE',  ( -13.16640216892762894, -18.94680327863774849, 11.49999999999998934 ) ) ;
#70909=CARTESIAN_POINT ( 'NONE',  ( -20.32193514540556123, 0.06534614623005505218, -1.500000000000002220 ) ) ;
#70913=CARTESIAN_POINT ( 'NONE',  ( -92.50481889294847804, -24.65952944569304961, 1.056160979905703901 ) ) ;
#70914=EDGE_CURVE ( 'NONE', #46454, #81148, #43585, .T. ) ;
#70915=DIRECTION ( 'NONE',  ( -0.000000000000000000, 2.173523156925979552E-06, -0.9999999999976378895 ) ) ;
#70917=CARTESIAN_POINT ( 'NONE',  ( -20.86232423683148340, -5.086641213604358391, 11.49999999999999645 ) ) ;
#70918=ORIENTED_EDGE ( 'NONE', *, *, #48369, .F. ) ;
#70920=CARTESIAN_POINT ( 'NONE',  ( -104.6228709571500559, -23.72747288104442021, -1.053458166803661999 ) ) ;
#70923=CARTESIAN_POINT ( 'NONE',  ( 19.40724743217988291, -7.346346906864608783, -1.500000000000002220 ) ) ;
#70924=EDGE_CURVE ( 'NONE', #80790, #86594, #89258, .T. ) ;
#70925=ORIENTED_EDGE ( 'NONE', *, *, #35012, .T. ) ;
#70926=CARTESIAN_POINT ( 'NONE',  ( -78.52287095715006160, -29.50247984919015209, -1.443849546365053582 ) ) ;
#70928=B_SPLINE_SURFACE_WITH_KNOTS ( 'NONE', 3, 1, ( 
 ( #12348, #2763 ),
 ( #74258, #96105 ),
 ( #4750, #35703 ),
 ( #57056, #18470 ),
 ( #64680, #11855 ),
 ( #96591, #28089 ),
 ( #95597, #26084 ),
 ( #87991, #66678 ),
 ( #27089, #10865 ),
 ( #34209, #88991 ),
 ( #41830, #88492 ),
 ( #58057, #80876 ),
 ( #18969, #49946 ),
 ( #35205, #66176 ),
 ( #27593, #58544 ),
 ( #89483, #19961 ),
 ( #91969, #37190 ),
 ( #82856, #5738 ),
 ( #74745, #44319 ) ),
 .UNSPECIFIED., .F., .F., .F.,
 ( 4, 1, 1, 1, 1, 1, 1, 1, 1, 1, 1, 1, 1, 1, 1, 1, 4 ),
 ( 2, 2 ),
 ( 0.000000000000000000, 0.07271299661694095862, 0.1415474849795007595, 0.2083625229559549763, 0.2724615839557062436, 0.3353899614876877933, 0.3977112986796186300, 0.4593833749474410810, 0.5220981738873415878, 0.5843147667471931817, 0.6443919352300537806, 0.7033450132947852707, 0.7615088749701885984, 0.8200304749172312446, 0.8785170367552999071, 0.9382645014876742628, 1.000000000000000000 ),
 ( 0.000000000000000000, 1.000000000000000000 ),
 .UNSPECIFIED. ) ;
#70929=CARTESIAN_POINT ( 'NONE',  ( -111.5570161281370076, -23.73791477778912551, 11.05961554403170055 ) ) ;
#70930=CARTESIAN_POINT ( 'NONE',  ( -102.6228709571500559, -29.50248528299804818, 1.056150453629042030 ) ) ;
#70933=DIRECTION ( 'NONE',  ( -0.4560907909095458512, 0.000000000000000000, 0.8899332505573128715 ) ) ;
#70934=CARTESIAN_POINT ( 'NONE',  ( -42.56929197859121672, -23.48786465467240347, 11.44779295918255535 ) ) ;
#70935=CARTESIAN_POINT ( 'NONE',  ( -43.58150547404529362, -24.51419770103157347, 9.386484678747178734 ) ) ;
#70936=CARTESIAN_POINT ( 'NONE',  ( 19.14557405504459453, -10.84957060938160289, 11.49999999999999645 ) ) ;
#70938=CARTESIAN_POINT ( 'NONE',  ( -4.885077187424587741, 22.05487924249641551, -1.500000000000002220 ) ) ;
#70940=CARTESIAN_POINT ( 'NONE',  ( -5.787726610425443674, -20.20099407548119075, 11.49999999999998934 ) ) ;
#70941=CARTESIAN_POINT ( 'NONE',  ( -70.62287095715008434, -23.84047902841601285, -0.8780736468305809783 ) ) ;
#70942=ORIENTED_EDGE ( 'NONE', *, *, #43721, .F. ) ;
#70943=VERTEX_POINT ( 'NONE', #80144 ) ;
#70945=AXIS2_PLACEMENT_3D ( 'NONE', #82870, #76251, #52941 ) ;
#70946=CARTESIAN_POINT ( 'NONE',  ( -113.6228709571500417, -23.47596703998600631, 11.44779298504227860 ) ) ;
#70947=ORIENTED_EDGE ( 'NONE', *, *, #81727, .F. ) ;
#70948=CARTESIAN_POINT ( 'NONE',  ( 21.03498508994548999, -2.205306954651367946, 11.49999999999998934 ) ) ;
#70949=CARTESIAN_POINT ( 'NONE',  ( -117.5895376238167245, -23.47593901973091235, -1.443836447538997536 ) ) ;
#70950=CARTESIAN_POINT ( 'NONE',  ( -51.54603119510975517, -25.03148648216341954, 7.131526314890322737 ) ) ;
#70951=CARTESIAN_POINT ( 'NONE',  ( -49.54496353273913201, -25.27887345932698082, 4.195367252302923511 ) ) ;
#70953=CARTESIAN_POINT ( 'NONE',  ( -79.58953762381672448, -24.64898659630528854, 1.056161002820827699 ) ) ;
#70955=CARTESIAN_POINT ( 'NONE',  ( 16.16129659511371131, 15.28805624652528472, -1.500000000000002220 ) ) ;
#70956=CARTESIAN_POINT ( 'NONE',  ( -49.57708068730813267, -25.03220865545371154, 7.373516867294396704 ) ) ;
#70957=ORIENTED_EDGE ( 'NONE', *, *, #88725, .T. ) ;
#70959=CARTESIAN_POINT ( 'NONE',  ( -48.62287095715004881, -24.50216790748097395, 0.6166512839513694777 ) ) ;
#70961=FACE_OUTER_BOUND ( 'NONE', #52094, .T. ) ;
#70963=CARTESIAN_POINT ( 'NONE',  ( -19.06185424839875964, 3.971334347869299286, -1.500000000000002220 ) ) ;
#70964=CARTESIAN_POINT ( 'NONE',  ( 4.431377227695222132, -20.94745169971119481, 11.49999999999998934 ) ) ;
#70966=CARTESIAN_POINT ( 'NONE',  ( -60.48283693452195564, -24.92592662360294042, 8.075495902990192931 ) ) ;
#70967=CARTESIAN_POINT ( 'NONE',  ( -51.55336426161518659, -23.96119346886880663, -0.6495511937832119109 ) ) ;
#70968=CARTESIAN_POINT ( 'NONE',  ( -121.6228709571500417, -29.50248528299804818, 1.056150453629045360 ) ) ;
#70969=CARTESIAN_POINT ( 'NONE',  ( 6.262736145392394427, -21.83385498489561272, -1.500000000000002220 ) ) ;
#70970=EDGE_CURVE ( 'NONE', #75118, #84956, #57332, .T. ) ;
#70971=CARTESIAN_POINT ( 'NONE',  ( -98.56082856698625960, -23.48783264082476663, -1.443836473390090136 ) ) ;
#70973=CARTESIAN_POINT ( 'NONE',  ( -13.56193660873917395, -14.51407242162769151, 11.49999999999999645 ) ) ;
#70974=CARTESIAN_POINT ( 'NONE',  ( -84.52287095715001897, -23.73907113216987952, -1.053371485793251461 ) ) ;
#70977=DIRECTION ( 'NONE',  ( -3.773278334453079030E-23, 0.9999999999976377785, 2.173523156925979128E-06 ) ) ;
#70978=ORIENTED_EDGE ( 'NONE', *, *, #47678, .T. ) ;
#70982=CARTESIAN_POINT ( 'NONE',  ( -71.52287095715007581, -24.50321055353805733, 9.387540953477515160 ) ) ;
#70983=CARTESIAN_POINT ( 'NONE',  ( -6.031157642910047301, -20.80930661755759203, 11.49999999999998934 ) ) ;
#70986=CARTESIAN_POINT ( 'NONE',  ( 2.628080361126900133, -19.32819128710564272, -1.500000000000002220 ) ) ;
#70988=CARTESIAN_POINT ( 'NONE',  ( -55.48558124947912518, -24.73531770709095312, 8.716586749053510275 ) ) ;
#70989=ORIENTED_EDGE ( 'NONE', *, *, #41828, .T. ) ;
#70990=ADVANCED_FACE ( 'NONE', ( #74035 ), #34474, .T. ) ;
#70991=CARTESIAN_POINT ( 'NONE',  ( 8.549789220347504326, 18.50885834720105905, 11.49999999999999645 ) ) ;
#70992=FACE_OUTER_BOUND ( 'NONE', #7484, .T. ) ;
#70993=EDGE_CURVE ( 'NONE', #82766, #2872, #15251, .T. ) ;
#70996=CARTESIAN_POINT ( 'NONE',  ( -34.52287095715006160, -29.50250786944525672, 11.44777988621624409 ) ) ;
#70997=PLANE ( 'NONE',  #60670 ) ;
#70998=CARTESIAN_POINT ( 'NONE',  ( -75.58953762381673869, -23.47596703998600276, 11.44779298504227683 ) ) ;
#71000=DIRECTION ( 'NONE',  ( -3.773278334444167608E-23, 1.000000000000000000, 0.000000000000000000 ) ) ;
#71001=CARTESIAN_POINT ( 'NONE',  ( 14.11618873683251252, 14.29484301466228047, 11.49999999999998934 ) ) ;
#71002=B_SPLINE_CURVE_WITH_KNOTS ( 'NONE', 3,
 ( #33175, #16950, #95080, #71752 ),
 .UNSPECIFIED., .F., .F.,
 ( 4, 4 ),
 ( 0.1806289827352041688, 0.1896354140073194250 ),
 .UNSPECIFIED. ) ;
#71003=CARTESIAN_POINT ( 'NONE',  ( -57.52287095715008292, -23.47593901973090524, -1.443836447538997092 ) ) ;
#71007=CARTESIAN_POINT ( 'NONE',  ( -14.98413761715186077, 17.36544542080599740, 11.49999999999999645 ) ) ;
#71008=CARTESIAN_POINT ( 'NONE',  ( -0.6305239314742796530, -22.70799625201654592, 11.49999999999998934 ) ) ;
#71009=ORIENTED_EDGE ( 'NONE', *, *, #87243, .F. ) ;
#71012=CARTESIAN_POINT ( 'NONE',  ( -38.64869433578421365, -23.96169478059712432, 10.65365249895718591 ) ) ;
#71013=CARTESIAN_POINT ( 'NONE',  ( -49.52287095715006160, -24.65952944569304606, 1.056160979905693686 ) ) ;
#71016=CARTESIAN_POINT ( 'NONE',  ( -49.20471335217622055, -25.31215404449747908, 5.309145496855610880 ) ) ;
#71017=CARTESIAN_POINT ( 'NONE',  ( -76.62287095715007013, -23.73934037231757443, 11.05740245334329153 ) ) ;
#71018=CARTESIAN_POINT ( 'NONE',  ( -98.90869474253671001, -25.25460678994682340, 5.895134505904293221 ) ) ;
#71019=ORIENTED_EDGE ( 'NONE', *, *, #30298, .F. ) ;
#71020=AXIS2_PLACEMENT_3D ( 'NONE', #339, #54640, #86076 ) ;
#71021=CARTESIAN_POINT ( 'NONE',  ( -10.90597124047809530, 17.21661415904998904, -1.500000000000002220 ) ) ;
#71022=ORIENTED_EDGE ( 'NONE', *, *, #76619, .T. ) ;
#71023=CARTESIAN_POINT ( 'NONE',  ( -12.88233675513024856, -19.01995677650982230, -1.500000000000002220 ) ) ;
#71026=CARTESIAN_POINT ( 'NONE',  ( -114.5228709571500190, -24.66019654487200441, 8.947790411086110396 ) ) ;
#71027=CARTESIAN_POINT ( 'NONE',  ( -101.5228709571500758, -23.47593901973090524, -1.443836447538996426 ) ) ;
#71029=AXIS2_PLACEMENT_3D ( 'NONE', #90826, #21300, #12193 ) ;
#71030=CARTESIAN_POINT ( 'NONE',  ( -1.825377252022436281, -21.23478267787193730, 11.49999999999999645 ) ) ;
#71031=EDGE_LOOP ( 'NONE', ( #12457, #1494, #96480, #97532 ) ) ;
#71033=CARTESIAN_POINT ( 'NONE',  ( -19.03210976516136554, 11.49075778266564107, -1.500000000000002220 ) ) ;
#71034=CARTESIAN_POINT ( 'NONE',  ( -14.43086120294938368, -14.79396848081076854, -1.500000000000002220 ) ) ;
#71035=EDGE_CURVE ( 'NONE', #95160, #12369, #13614, .T. ) ;
#71038=EDGE_CURVE ( 'NONE', #43355, #8583, #5549, .T. ) ;
#71039=CARTESIAN_POINT ( 'NONE',  ( -95.54220200439495159, -25.00182538069147142, 7.747789668545043362 ) ) ;
#71041=CARTESIAN_POINT ( 'NONE',  ( -79.62287095715005592, -23.48786465467241058, 11.44779295918254469 ) ) ;
#71044=CARTESIAN_POINT ( 'NONE',  ( -70.62963902551980766, -25.12997664719427959, 7.061473379948721707 ) ) ;
#71045=CARTESIAN_POINT ( 'NONE',  ( 19.40856703110355852, -7.758221025823637262, -1.500000000000002220 ) ) ;
#71046=CARTESIAN_POINT ( 'NONE',  ( -1.678574117887026373, -21.80011532881206548, 11.49999999999999645 ) ) ;
#71049=CARTESIAN_POINT ( 'NONE',  ( 14.32739804834607256, 17.34395043298086847, -1.500000000000002220 ) ) ;
#71050=CARTESIAN_POINT ( 'NONE',  ( -118.5546831409418616, -24.15620529776628800, 10.23563542870659759 ) ) ;
#71051=B_SPLINE_CURVE_WITH_KNOTS ( 'NONE', 3,
 ( #10688, #71594, #32016, #94416 ),
 .UNSPECIFIED., .F., .F.,
 ( 4, 4 ),
 ( 0.3700501682448147367, 0.3790565995169303259 ),
 .UNSPECIFIED. ) ;
#71052=CARTESIAN_POINT ( 'NONE',  ( -57.62287095715004881, -24.64898659630367916, 1.056161002820822592 ) ) ;
#71053=CARTESIAN_POINT ( 'NONE',  ( -78.52287095715004739, -23.48783264082476308, -1.443836473390091468 ) ) ;
#71054=VERTEX_POINT ( 'NONE', #52198 ) ;
#71055=B_SPLINE_SURFACE_WITH_KNOTS ( 'NONE', 3, 3, ( 
 ( #42785, #51889, #73717, #27555 ),
 ( #75206, #4212, #51384, #82816 ),
 ( #82325, #29527, #67616, #6694 ),
 ( #60008, #37648, #91931, #84315 ),
 ( #46769, #99031, #83315, #13798 ),
 ( #100018, #98534, #14797, #76198 ),
 ( #30025, #54384, #91423, #68603 ),
 ( #45763, #45271, #36651, #23398 ),
 ( #29030, #85313, #99527, #76686 ),
 ( #21406, #52382, #15300, #31030 ) ),
 .UNSPECIFIED., .F., .F., .F.,
 ( 4, 3, 3, 4 ),
 ( 4, 4 ),
 ( 0.0004766839783813280377, 0.1491231665100169190, 0.2234464077758346878, 0.2977696490416524844 ),
 ( 0.7495845312173156083, 0.7510439293833934826 ),
 .UNSPECIFIED. ) ;
#71057=ORIENTED_EDGE ( 'NONE', *, *, #42014, .F. ) ;
#71061=VERTEX_POINT ( 'NONE', #6011 ) ;
#71062=CARTESIAN_POINT ( 'NONE',  ( -7.638042729800005759, 19.97414216180626667, -1.500000000000002220 ) ) ;
#71063=CARTESIAN_POINT ( 'NONE',  ( 21.65046080595755740, -5.567969076317650590, 11.49999999999999645 ) ) ;
#71064=ORIENTED_EDGE ( 'NONE', *, *, #6793, .T. ) ;
#71065=DIRECTION ( 'NONE',  ( -3.773278334444167608E-23, 1.000000000000000000, 0.000000000000000000 ) ) ;
#71066=CARTESIAN_POINT ( 'NONE',  ( -1.165634184549018126, -21.02984315360824752, -1.500000000000002220 ) ) ;
#71067=CARTESIAN_POINT ( 'NONE',  ( -30.54633378701636559, -24.57840743580478104, 9.174392229302920754 ) ) ;
#71068=CARTESIAN_POINT ( 'NONE',  ( -19.95764006394758638, 0.7380318605572177004, -1.500000000000002220 ) ) ;
#71069=CARTESIAN_POINT ( 'NONE',  ( -114.6228709571500417, -23.48786465467241769, 11.44779295918253936 ) ) ;
#71071=CARTESIAN_POINT ( 'NONE',  ( -14.32918165687622825, -16.72005635474405949, -1.500000000000002220 ) ) ;
#71072=FACE_OUTER_BOUND ( 'NONE', #5391, .T. ) ;
#71073=ORIENTED_EDGE ( 'NONE', *, *, #26054, .F. ) ;
#71074=CARTESIAN_POINT ( 'NONE',  ( -65.53038835011091123, -25.00182538069146432, 7.747789668545041586 ) ) ;
#71076=CARTESIAN_POINT ( 'NONE',  ( 12.78316523911058944, -16.47895720935621711, 11.49999999999999645 ) ) ;
#71077=VECTOR ( 'NONE', #42050, 1000.000000000000114 ) ;
#71078=CARTESIAN_POINT ( 'NONE',  ( -74.55620429048340725, -24.65952944569304606, 1.056160979905698571 ) ) ;
#71079=CARTESIAN_POINT ( 'NONE',  ( -108.6228709571500559, -23.73934037231757799, 11.05740245334328087 ) ) ;
#71081=CARTESIAN_POINT ( 'NONE',  ( -10.68834330497911189, 18.46263264838738039, -1.500000000000002220 ) ) ;
#71083=CARTESIAN_POINT ( 'NONE',  ( -50.66585102988210565, -25.19861947315626693, 3.319393630720075095 ) ) ;
#71086=CARTESIAN_POINT ( 'NONE',  ( 16.80569330386292748, 14.95695114220347932, -1.500000000000002220 ) ) ;
#71087=B_SPLINE_CURVE_WITH_KNOTS ( 'NONE', 3,
 ( #58350, #12650, #89285, #96395, #50728, #35990 ),
 .UNSPECIFIED., .F., .F.,
 ( 4, 2, 4 ),
 ( 1.570755371633836552E-05, 0.001396183895866086018, 0.002776660238015833410 ),
 .UNSPECIFIED. ) ;
#71089=EDGE_LOOP ( 'NONE', ( #63808, #87948, #8532, #51477 ) ) ;
#71092=CARTESIAN_POINT ( 'NONE',  ( 5.239555828037883778, -18.94419173073049478, 11.49999999999999645 ) ) ;
#71093=PLANE ( 'NONE',  #52095 ) ;
#71094=B_SPLINE_CURVE_WITH_KNOTS ( 'NONE', 3,
 ( #87845, #27941, #88854, #72132, #18330, #19319 ),
 .UNSPECIFIED., .F., .F.,
 ( 4, 2, 4 ),
 ( 0.000000000000000000, 0.001380901958385385509, 0.002761803916770771018 ),
 .UNSPECIFIED. ) ;
#71096=CARTESIAN_POINT ( 'NONE',  ( -119.5228709571500900, -23.72773821059536914, 11.05748984161097326 ) ) ;
#71097=EDGE_LOOP ( 'NONE', ( #12641, #99462, #10110, #43456 ) ) ;
#71098=CARTESIAN_POINT ( 'NONE',  ( -99.50979288673286760, -24.51314013834316796, 0.6176544820404243907 ) ) ;
#71099=CARTESIAN_POINT ( 'NONE',  ( -99.58953762381672448, -24.66019654487198665, 8.947790411086137041 ) ) ;
#71101=CARTESIAN_POINT ( 'NONE',  ( -105.5228709571500758, -25.00182538069145366, 7.747789668545101094 ) ) ;
#71103=CARTESIAN_POINT ( 'NONE',  ( -5.448126336921106372, -18.99418723138115084, -1.500000000000002220 ) ) ;
#71105=EDGE_CURVE ( 'NONE', #58964, #92752, #99353, .T. ) ;
#71106=CARTESIAN_POINT ( 'NONE',  ( 4.066846734877469949, -19.79409818376439389, 11.49999999999999645 ) ) ;
#71108=ADVANCED_FACE ( 'NONE', ( #36965 ), #82272, .T. ) ;
#71110=CARTESIAN_POINT ( 'NONE',  ( -48.62287095715007723, -23.95044443724991012, 10.65354141964650125 ) ) ;
#71112=CARTESIAN_POINT ( 'NONE',  ( -50.37830952628070946, -25.30401792888237367, 5.197789011716579033 ) ) ;
#71114=CARTESIAN_POINT ( 'NONE',  ( -129.6228709571500417, -29.50248528299804818, 1.056150453629047137 ) ) ;
#71115=CARTESIAN_POINT ( 'NONE',  ( -107.5489772126510530, -24.65952944569305316, 1.056160979905704789 ) ) ;
#71116=CARTESIAN_POINT ( 'NONE',  ( -19.89792590360708147, -2.209704250470923892, -1.500000000000002220 ) ) ;
#71117=EDGE_CURVE ( 'NONE', #50685, #17220, #64900, .T. ) ;
#71118=CARTESIAN_POINT ( 'NONE',  ( -99.29064586046420970, -25.10935166775642813, 3.426411013435906039 ) ) ;
#71119=CARTESIAN_POINT ( 'NONE',  ( -116.5525123351993955, -24.51419770103160189, 9.386484678747169852 ) ) ;
#71121=CARTESIAN_POINT ( 'NONE',  ( -79.60031018295994443, -23.73791477778911840, 11.05961554403170943 ) ) ;
#71122=CARTESIAN_POINT ( 'NONE',  ( -109.6405337342305302, -25.29012783774154016, 3.562353256831511494 ) ) ;
#71123=CARTESIAN_POINT ( 'NONE',  ( -35.47208223784672754, -24.83618233451450052, 1.606449574219543708 ) ) ;
#71124=CARTESIAN_POINT ( 'NONE',  ( -48.62287095715004881, -24.64965695001467694, 8.947790433994185832 ) ) ;
#71126=CARTESIAN_POINT ( 'NONE',  ( -83.56309348553224936, -23.48783264082477018, -1.443836473390093689 ) ) ;
#71128=CARTESIAN_POINT ( 'NONE',  ( -50.19347037116831700, -25.18630682891961214, 3.303495449920700544 ) ) ;
#71132=CARTESIAN_POINT ( 'NONE',  ( 13.48481281434462531, 15.16087405922196041, -1.500000000000002220 ) ) ;
#71134=CARTESIAN_POINT ( 'NONE',  ( -34.58677685350260589, -24.34968618360933590, 0.1864209137778841396 ) ) ;
#71136=CARTESIAN_POINT ( 'NONE',  ( -59.62366543129058982, -24.66019654487199730, 8.947790411086124607 ) ) ;
#71140=CARTESIAN_POINT ( 'NONE',  ( -5.623992922573770592, 19.38241096367466199, -1.500000000000002220 ) ) ;
#71141=CARTESIAN_POINT ( 'NONE',  ( -18.69274626484788371, 9.848020819832786543, 11.49999999999999645 ) ) ;
#71142=VECTOR ( 'NONE', #57038, 1000.000000000000114 ) ;
#71143=CARTESIAN_POINT ( 'NONE',  ( -13.50798789833325664, 17.53495777034937220, 11.49999999999998934 ) ) ;
#71145=CARTESIAN_POINT ( 'NONE',  ( -20.42507745660439156, -2.452541965221147535, -1.500000000000002220 ) ) ;
#71146=CARTESIAN_POINT ( 'NONE',  ( -44.62287095715004881, -29.50250243563736774, 8.947779886222148704 ) ) ;
#71147=ORIENTED_EDGE ( 'NONE', *, *, #41956, .F. ) ;
#71149=ORIENTED_EDGE ( 'NONE', *, *, #97881, .F. ) ;
#71151=CARTESIAN_POINT ( 'NONE',  ( -61.62287095715004881, -23.48786465467240347, 11.44779295918254824 ) ) ;
#71152=VERTEX_POINT ( 'NONE', #84133 ) ;
#71153=ORIENTED_EDGE ( 'NONE', *, *, #51906, .T. ) ;
#71154=VECTOR ( 'NONE', #30317, 1000.000000000000114 ) ;
#71155=ORIENTED_EDGE ( 'NONE', *, *, #56177, .F. ) ;
#71156=CARTESIAN_POINT ( 'NONE',  ( -47.52287095715006160, -23.47596703998600631, 11.44779298504229104 ) ) ;
#71159=CARTESIAN_POINT ( 'NONE',  ( 16.58470376584361361, 12.37529123428901556, -1.500000000000002220 ) ) ;
#71160=CARTESIAN_POINT ( 'NONE',  ( 16.85579979752674618, 13.57973486276658903, 11.49999999999999645 ) ) ;
#71161=ORIENTED_EDGE ( 'NONE', *, *, #3086, .F. ) ;
#71162=CARTESIAN_POINT ( 'NONE',  ( -99.16166289166535819, -25.30166215957521914, 5.311370747606397380 ) ) ;
#71163=CARTESIAN_POINT ( 'NONE',  ( -110.3139465455115129, -25.11033443737754212, 2.832404817301930056 ) ) ;
#71164=CARTESIAN_POINT ( 'NONE',  ( 20.53814608839396527, -8.957171556794316203, 11.49999999999998934 ) ) ;
#71165=CARTESIAN_POINT ( 'NONE',  ( -79.36551648466291908, -25.27874893558202984, 6.194053881209717893 ) ) ;
#71166=CARTESIAN_POINT ( 'NONE',  ( -53.52287095715006160, -24.50216790748205042, 0.6166512839542438451 ) ) ;
#71167=ORIENTED_EDGE ( 'NONE', *, *, #78387, .T. ) ;
#71169=CARTESIAN_POINT ( 'NONE',  ( -76.62287095715007013, -23.72773821059535848, 11.05748984161097681 ) ) ;
#71170=B_SPLINE_CURVE_WITH_KNOTS ( 'NONE', 3,
 ( #39168, #40685, #78711, #609 ),
 .UNSPECIFIED., .F., .F.,
 ( 4, 4 ),
 ( 0.8403860235663986877, 0.8493924548385139994 ),
 .UNSPECIFIED. ) ;
#71171=ORIENTED_EDGE ( 'NONE', *, *, #82475, .F. ) ;
#71172=VERTEX_POINT ( 'NONE', #99841 ) ;
#71173=CARTESIAN_POINT ( 'NONE',  ( -70.58953762381671027, -23.48783264082478084, -1.443836473390067265 ) ) ;
#71175=ORIENTED_EDGE ( 'NONE', *, *, #10843, .F. ) ;
#71177=CARTESIAN_POINT ( 'NONE',  ( -108.2228709571500644, -23.47593901973090169, -1.443836447538996648 ) ) ;
#71178=CARTESIAN_POINT ( 'NONE',  ( 17.84191302092929021, 11.53353326677314961, -1.500000000000002220 ) ) ;
#71179=ORIENTED_EDGE ( 'NONE', *, *, #28565, .T. ) ;
#71180=DIRECTION ( 'NONE',  ( -3.773278334453079030E-23, 0.9999999999976377785, 2.173523156925979128E-06 ) ) ;
#71181=CARTESIAN_POINT ( 'NONE',  ( -1.534710021792092594, -21.76038796025502009, -1.500000000000002220 ) ) ;
#71182=CARTESIAN_POINT ( 'NONE',  ( -52.63305254789141685, -24.35071581493542681, 9.817618358456035921 ) ) ;
#71183=CARTESIAN_POINT ( 'NONE',  ( -63.62287095715004881, -29.50250786944525672, 11.44777988621623876 ) ) ;
#71184=FACE_OUTER_BOUND ( 'NONE', #71774, .T. ) ;
#71185=CARTESIAN_POINT ( 'NONE',  ( 10.97640485992876691, 18.82695874702771377, -1.500000000000002220 ) ) ;
#71186=CARTESIAN_POINT ( 'NONE',  ( -95.52287095715001897, -23.85196035786900026, -0.8779234886475105748 ) ) ;
#71187=VERTEX_POINT ( 'NONE', #24733 ) ;
#71188=CARTESIAN_POINT ( 'NONE',  ( -63.62287095715004881, -24.64898659630528499, 1.056161002820822592 ) ) ;
#71189=CARTESIAN_POINT ( 'NONE',  ( -48.87479414115020404, -25.12782512515361333, 6.180417935526588025 ) ) ;
#71190=VERTEX_POINT ( 'NONE', #47594 ) ;
#71191=EDGE_CURVE ( 'NONE', #21474, #29757, #100336, .T. ) ;
#71194=CARTESIAN_POINT ( 'NONE',  ( -47.62287095715004881, -29.50250786944525672, 11.44777988621624054 ) ) ;
#71195=CARTESIAN_POINT ( 'NONE',  ( -82.50601559517893691, -24.34968618360933945, 0.1864209137778926328 ) ) ;
#71196=CARTESIAN_POINT ( 'NONE',  ( 14.73992482348874411, 15.29747818672187165, 11.49999999999998934 ) ) ;
#71197=CARTESIAN_POINT ( 'NONE',  ( -94.56143254526521957, -23.48783264082477018, -1.443836473390086805 ) ) ;
#71198=CARTESIAN_POINT ( 'NONE',  ( -130.5728709571500588, -24.45056191361607389, 9.787827635114014768 ) ) ;
#71199=CARTESIAN_POINT ( 'NONE',  ( -41.62287095715006302, -23.47593901973091235, -1.443836447539011525 ) ) ;
#71200=CARTESIAN_POINT ( 'NONE',  ( -99.52287095715004739, -24.50216790748204687, 0.6166512839542553914 ) ) ;
#71201=CARTESIAN_POINT ( 'NONE',  ( -1.608633542659107629, -19.34071428503001755, 11.49999999999998934 ) ) ;
#71202=CARTESIAN_POINT ( 'NONE',  ( -107.6228709571500701, -24.65952944569304961, 1.056160979905703901 ) ) ;
#71203=ORIENTED_EDGE ( 'NONE', *, *, #30299, .F. ) ;
#71204=CARTESIAN_POINT ( 'NONE',  ( 15.68791110202092476, 11.56419973807686219, 11.49999999999999645 ) ) ;
#71209=ORIENTED_EDGE ( 'NONE', *, *, #54991, .F. ) ;
#71211=CARTESIAN_POINT ( 'NONE',  ( -89.50838371253736625, -24.34968618360934300, 0.1864209137778942982 ) ) ;
#71213=CARTESIAN_POINT ( 'NONE',  ( -91.62287095715004170, -24.50321055353805733, 9.387540953477524042 ) ) ;
#71214=CARTESIAN_POINT ( 'NONE',  ( -101.0590973978295466, -25.21362872155826551, 3.509685239648734800 ) ) ;
#71215=CARTESIAN_POINT ( 'NONE',  ( -19.67010641940559168, 0.002901314006966619011, -1.500000000000002220 ) ) ;
#71217=ORIENTED_EDGE ( 'NONE', *, *, #17399, .T. ) ;
#71218=CARTESIAN_POINT ( 'NONE',  ( -4.019545577234938882, 21.20919285897865336, 11.49999999999998934 ) ) ;
#71220=AXIS2_PLACEMENT_3D ( 'NONE', #13706, #84724, #6103 ) ;
#71221=CARTESIAN_POINT ( 'NONE',  ( -65.62287095715005592, -25.00182538069145721, 7.747789668545100206 ) ) ;
#71222=CARTESIAN_POINT ( 'NONE',  ( 22.95697726795019378, -2.620641032420567118, -1.500000000000002220 ) ) ;
#71223=EDGE_CURVE ( 'NONE', #12270, #87638, #46588, .T. ) ;
#71224=VECTOR ( 'NONE', #21610, 1000.000000000000114 ) ;
#71228=CARTESIAN_POINT ( 'NONE',  ( -29.52287095715007581, -24.25489487036892200, 9.819270455405353815 ) ) ;
#71229=CARTESIAN_POINT ( 'NONE',  ( -128.6228709571500417, -23.47596703998600631, 11.44779298504227860 ) ) ;
#71231=CARTESIAN_POINT ( 'NONE',  ( -129.5900271110918709, -23.48783264082478084, -1.443836473390078590 ) ) ;
#71232=CARTESIAN_POINT ( 'NONE',  ( -99.25286268653823640, -25.31566011607329258, 4.527133398161728550 ) ) ;
#71233=CARTESIAN_POINT ( 'NONE',  ( -14.97016004668225264, 13.15154794113874637, -1.500000000000002220 ) ) ;
#71235=CARTESIAN_POINT ( 'NONE',  ( -75.53432623487223907, -25.00182538069146787, 7.747789668545045139 ) ) ;
#71236=CARTESIAN_POINT ( 'NONE',  ( 13.50462702941046977, 14.53317887778067252, -1.500000000000002220 ) ) ;
#71237=ORIENTED_EDGE ( 'NONE', *, *, #25480, .T. ) ;
#71238=FACE_OUTER_BOUND ( 'NONE', #49394, .T. ) ;
#71239=B_SPLINE_CURVE_WITH_KNOTS ( 'NONE', 3,
 ( #26566, #2735, #96560, #80849 ),
 .UNSPECIFIED., .F., .F.,
 ( 4, 4 ),
 ( 0.000000000000000000, 9.999999999997510880E-05 ),
 .UNSPECIFIED. ) ;
#71240=CARTESIAN_POINT ( 'NONE',  ( -51.39797819248544641, -25.20552468222252074, 6.636430008107547351 ) ) ;
#71242=CARTESIAN_POINT ( 'NONE',  ( -9.565632364391108311, -18.43008791299702764, 11.49999999999999645 ) ) ;
#71244=CARTESIAN_POINT ( 'NONE',  ( -78.52287095715006160, -24.64965694238408034, 8.947790433994198267 ) ) ;
#71245=CARTESIAN_POINT ( 'NONE',  ( -0.9122204482399535186, 22.77315974801211240, 11.49999999999999645 ) ) ;
#71247=CARTESIAN_POINT ( 'NONE',  ( -69.52210430107112415, -23.48783264082476308, -1.443836473390097908 ) ) ;
#71248=DIRECTION ( 'NONE',  ( 0.000000000000000000, -2.173523156925980399E-06, 0.9999999999976378895 ) ) ;
#71250=CARTESIAN_POINT ( 'NONE',  ( -9.470923242388245455, -17.85692771776473364, 11.49999999999998934 ) ) ;
#71252=CARTESIAN_POINT ( 'NONE',  ( -108.6228709571500417, -24.66019654487199730, 8.947790411086124607 ) ) ;
#71254=FACE_OUTER_BOUND ( 'NONE', #84030, .T. ) ;
#71255=CARTESIAN_POINT ( 'NONE',  ( -10.62949710387652758, 20.32685691788189075, 11.49999999999998934 ) ) ;
#71257=CARTESIAN_POINT ( 'NONE',  ( -19.26508835251014773, 5.270845654819066084, -1.500000000000002220 ) ) ;
#71259=CARTESIAN_POINT ( 'NONE',  ( 10.18035917307295435, 18.35650967997132099, 11.49999999999999645 ) ) ;
#71260=CARTESIAN_POINT ( 'NONE',  ( -29.81175120719462512, -25.25636103033882307, 4.942810967025194735 ) ) ;
#71262=CARTESIAN_POINT ( 'NONE',  ( -3.902479932019291553, -21.71820464621639246, 11.49999999999998934 ) ) ;
#71265=EDGE_CURVE ( 'NONE', #28831, #97694, #91434, .T. ) ;
#71266=ORIENTED_EDGE ( 'NONE', *, *, #5921, .F. ) ;
#71267=CARTESIAN_POINT ( 'NONE',  ( -127.5562042904833646, -23.48786465467242124, 11.44779295918252870 ) ) ;
#71268=CARTESIAN_POINT ( 'NONE',  ( -49.50841769935764347, -25.27344909660374839, 3.984447732001930920 ) ) ;
#71269=CARTESIAN_POINT ( 'NONE',  ( -102.6228709571500701, -24.66019654487199730, 8.947790411086121054 ) ) ;
#71271=CARTESIAN_POINT ( 'NONE',  ( -123.6228709571500417, -24.50321055353804667, 9.387540953477525818 ) ) ;
#71274=B_SPLINE_CURVE_WITH_KNOTS ( 'NONE', 3,
 ( #63942, #2522, #86740, #38678 ),
 .UNSPECIFIED., .F., .F.,
 ( 4, 4 ),
 ( 0.000000000000000000, 0.0001000000000000028644 ),
 .UNSPECIFIED. ) ;
#71275=ORIENTED_EDGE ( 'NONE', *, *, #70640, .F. ) ;
#71276=DIRECTION ( 'NONE',  ( -3.773278334453079618E-23, 0.9999999999976377785, 2.173523156925978705E-06 ) ) ;
#71277=CARTESIAN_POINT ( 'NONE',  ( -43.52287095715006160, -29.50248528299804818, 1.056150453629031594 ) ) ;
#71278=CARTESIAN_POINT ( 'NONE',  ( -94.62287095715005592, -24.50321055353806798, 9.387540953477534700 ) ) ;
#71279=CARTESIAN_POINT ( 'NONE',  ( 11.93631617611541351, -16.73449621718459923, -1.500000000000002220 ) ) ;
#71281=CARTESIAN_POINT ( 'NONE',  ( -63.52287095715006160, -24.66019654487199375, 8.947790411086122830 ) ) ;
#71283=CARTESIAN_POINT ( 'NONE',  ( -44.55313127954051566, -23.96119346886879953, -0.6495511937832129101 ) ) ;
#71285=CARTESIAN_POINT ( 'NONE',  ( -21.62769966018443313, 5.350386031573528989, -1.500000000000002220 ) ) ;
#71286=CARTESIAN_POINT ( 'NONE',  ( -0.1051205485391841221, -21.68913189117569473, 10.47594215909544246 ) ) ;
#71288=VERTEX_POINT ( 'NONE', #86640 ) ;
#71289=CARTESIAN_POINT ( 'NONE',  ( -96.62287095715004170, -23.73907113216991860, -1.053371485793224149 ) ) ;
#71290=VECTOR ( 'NONE', #52553, 1000.000000000000114 ) ;
#71293=CARTESIAN_POINT ( 'NONE',  ( -10.15938669249390180, 18.18672505111813464, 11.49999999999998934 ) ) ;
#71294=VERTEX_POINT ( 'NONE', #31353 ) ;
#71295=CARTESIAN_POINT ( 'NONE',  ( -116.5228709571500616, -24.65952944569305316, 1.056160979905705899 ) ) ;
#71298=ORIENTED_EDGE ( 'NONE', *, *, #41309, .T. ) ;
#71299=AXIS2_PLACEMENT_3D ( 'NONE', #97029, #57990, #51360 ) ;
#71300=CARTESIAN_POINT ( 'NONE',  ( -68.93918693012690824, -25.03149073271524117, 6.184868930986158198 ) ) ;
#71301=CARTESIAN_POINT ( 'NONE',  ( -10.24336464640716216, -18.35016636821181280, -1.500000000000002220 ) ) ;
#71302=ORIENTED_EDGE ( 'NONE', *, *, #58491, .T. ) ;
#71303=CARTESIAN_POINT ( 'NONE',  ( -110.6228709571500701, -24.82558206586150717, 1.605769216559632895 ) ) ;
#71304=CARTESIAN_POINT ( 'NONE',  ( -49.68570927577133745, -25.30558383668931910, 4.971112481134402294 ) ) ;
#71306=ADVANCED_FACE ( 'NONE', ( #8013 ), #79019, .T. ) ;
#71307=CARTESIAN_POINT ( 'NONE',  ( -101.7635726060833434, -25.25419390327883562, 6.809096110917860933 ) ) ;
#71308=CARTESIAN_POINT ( 'NONE',  ( -59.58303446354969424, -24.51314013834316441, 0.6176544820404136216 ) ) ;
#71310=DIRECTION ( 'NONE',  ( 0.000000000000000000, 0.9999999999976377785, 2.173523156925979975E-06 ) ) ;
#71311=CARTESIAN_POINT ( 'NONE',  ( -22.15176777451872425, 1.842445310382735624, 11.49999999999999645 ) ) ;
#71315=ORIENTED_EDGE ( 'NONE', *, *, #58676, .F. ) ;
#71316=CARTESIAN_POINT ( 'NONE',  ( 9.629844747126790949, -20.51516216672183290, -1.500000000000002220 ) ) ;
#71320=ORIENTED_EDGE ( 'NONE', *, *, #10524, .F. ) ;
#71322=EDGE_CURVE ( 'NONE', #37450, #62739, #86140, .T. ) ;
#71323=CARTESIAN_POINT ( 'NONE',  ( -47.62287095715004881, -24.64965695001467694, 8.947790433994185832 ) ) ;
#71324=B_SPLINE_CURVE_WITH_KNOTS ( 'NONE', 3,
 ( #94539, #24021, #39747, #47878 ),
 .UNSPECIFIED., .F., .F.,
 ( 4, 4 ),
 ( 0.000000000000000000, 1.000000000000000000 ),
 .UNSPECIFIED. ) ;
#71325=CARTESIAN_POINT ( 'NONE',  ( 14.24339680280927567, 14.23919408161895284, -1.500000000000002220 ) ) ;
#71326=DIRECTION ( 'NONE',  ( -3.773278334453079618E-23, 0.9999999999976377785, 2.173523156925979975E-06 ) ) ;
#71327=ORIENTED_EDGE ( 'NONE', *, *, #12649, .F. ) ;
#71328=PLANE ( 'NONE',  #63343 ) ;
#71329=CARTESIAN_POINT ( 'NONE',  ( -18.60458529277170214, -12.42720982490441095, -1.500000000000002220 ) ) ;
#71331=ORIENTED_EDGE ( 'NONE', *, *, #36622, .T. ) ;
#71332=ORIENTED_EDGE ( 'NONE', *, *, #80739, .T. ) ;
#71334=CARTESIAN_POINT ( 'NONE',  ( -122.5228709571500616, -29.50247984919015209, -1.443849546365046699 ) ) ;
#71335=CARTESIAN_POINT ( 'NONE',  ( -41.52287095715005449, -23.96127896942119051, -0.6493128930941884924 ) ) ;
#71336=CARTESIAN_POINT ( 'NONE',  ( -97.26334014122947735, -23.47593901973090524, -1.443836447538996648 ) ) ;
#71337=CARTESIAN_POINT ( 'NONE',  ( -18.23851433863309879, 7.102826447048048664, 11.49999999999998934 ) ) ;
#71338=PLANE ( 'NONE',  #16616 ) ;
#71339=ORIENTED_EDGE ( 'NONE', *, *, #18955, .F. ) ;
#71340=CARTESIAN_POINT ( 'NONE',  ( 16.48747857468482891, 13.79107804547330929, 11.49999999999998934 ) ) ;
#71342=CARTESIAN_POINT ( 'NONE',  ( -54.62287095715004170, -24.33927499327855060, 9.819080762295818943 ) ) ;
#71343=CARTESIAN_POINT ( 'NONE',  ( -63.52287095715006160, -24.66019654487199375, 8.947790411086122830 ) ) ;
#71344=VECTOR ( 'NONE', #59177, 1000.000000000000114 ) ;
#71345=CARTESIAN_POINT ( 'NONE',  ( -111.6228709571500701, -23.96127896941633750, -0.6493128931037791540 ) ) ;
#71346=CARTESIAN_POINT ( 'NONE',  ( -0.4961427919413599064, 22.93664481792237453, -1.500000000000002220 ) ) ;
#71347=EDGE_CURVE ( 'NONE', #26963, #12709, #97563, .T. ) ;
#71348=EDGE_CURVE ( 'NONE', #73913, #81354, #54705, .T. ) ;
#71351=CARTESIAN_POINT ( 'NONE',  ( -70.66096558152140972, -25.31062324876412006, 5.350544532130630415 ) ) ;
#71352=CARTESIAN_POINT ( 'NONE',  ( -20.00956492049148494, -0.6725752471728385640, 11.49999999999999645 ) ) ;
#71353=CARTESIAN_POINT ( 'NONE',  ( -79.16633218095056179, -25.26612511361882341, 5.138964462063473349 ) ) ;
#71357=CARTESIAN_POINT ( 'NONE',  ( -65.55620429048339304, -23.47593901973091235, -1.443836447539006196 ) ) ;
#71358=EDGE_CURVE ( 'NONE', #97163, #79765, #63620, .T. ) ;
#71359=CARTESIAN_POINT ( 'NONE',  ( 14.05712878599199200, -16.60762996970646199, 11.49999999999998934 ) ) ;
#71361=CARTESIAN_POINT ( 'NONE',  ( -6.620539020842763911, -18.51205181221761720, -1.500000000000002220 ) ) ;
#71363=EDGE_CURVE ( 'NONE', #57842, #29757, #81745, .T. ) ;
#71370=CARTESIAN_POINT ( 'NONE',  ( -102.5228709571501042, -23.48783264083375144, -1.443836473376139740 ) ) ;
#71371=CARTESIAN_POINT ( 'NONE',  ( 18.12345787009687115, -9.690629616749632191, 11.49999999999999645 ) ) ;
#71374=VECTOR ( 'NONE', #22636, 1000.000000000000114 ) ;
#71375=CARTESIAN_POINT ( 'NONE',  ( 0.2737972009257602091, 22.58959237946467624, 11.49999999999999645 ) ) ;
#71376=VERTEX_POINT ( 'NONE', #87650 ) ;
#71378=CARTESIAN_POINT ( 'NONE',  ( -69.94684934828960365, -25.25639587450186951, 7.037048054415059539 ) ) ;
#71380=CARTESIAN_POINT ( 'NONE',  ( -97.54780332990628722, -24.51314013834316086, 0.6176544820404162861 ) ) ;
#71381=CARTESIAN_POINT ( 'NONE',  ( -72.62287095715005592, -24.64965695001468404, 8.947790433994184056 ) ) ;
#71382=CARTESIAN_POINT ( 'NONE',  ( -25.53444008324515124, -24.93062977454840023, 5.226875182649808771 ) ) ;
#71383=FACE_OUTER_BOUND ( 'NONE', #41653, .T. ) ;
#71384=ORIENTED_EDGE ( 'NONE', *, *, #96206, .T. ) ;
#71386=CARTESIAN_POINT ( 'NONE',  ( -22.75767140345847750, 1.815691853630000629, 11.49999999999998934 ) ) ;
#71387=CARTESIAN_POINT ( 'NONE',  ( -69.52287095715006160, -23.47596703998600631, 11.44779298504228748 ) ) ;
#71388=CARTESIAN_POINT ( 'NONE',  ( -96.51332711276727139, -24.15543982623907482, -0.2315651400026596807 ) ) ;
#71390=CARTESIAN_POINT ( 'NONE',  ( 3.433349652534986696, 22.22849440524942111, 11.49999999999999645 ) ) ;
#71392=CARTESIAN_POINT ( 'NONE',  ( -43.61623332758254179, -23.48783264082478084, -1.443836473390076369 ) ) ;
#71393=CARTESIAN_POINT ( 'NONE',  ( 14.12621959167996977, 16.79361087625908056, -1.500000000000002220 ) ) ;
#71395=CARTESIAN_POINT ( 'NONE',  ( -34.66748501521039572, -23.48786465467240347, 11.44779295918255535 ) ) ;
#71401=CARTESIAN_POINT ( 'NONE',  ( -8.751980504941329286, -18.49744413911281882, 11.49999999999998934 ) ) ;
#71405=ORIENTED_EDGE ( 'NONE', *, *, #66142, .T. ) ;
#71406=CARTESIAN_POINT ( 'NONE',  ( 22.95697726795019378, -2.620641032420567118, -1.500000000000002220 ) ) ;
#71407=CARTESIAN_POINT ( 'NONE',  ( -102.6228709571500701, -24.66019654487199730, 8.947790411086121054 ) ) ;
#71408=CARTESIAN_POINT ( 'NONE',  ( 3.729398819442638846, -20.01364129133569136, -1.500000000000002220 ) ) ;
#71409=ORIENTED_EDGE ( 'NONE', *, *, #98325, .T. ) ;
#71412=DIRECTION ( 'NONE',  ( -1.000000000000000000, -3.773278334444166432E-23, -8.201307841325785021E-29 ) ) ;
#71414=CARTESIAN_POINT ( 'NONE',  ( 19.32660459246815421, -9.429101867163046435, 11.49999999999999645 ) ) ;
#71416=CARTESIAN_POINT ( 'NONE',  ( -75.63151842343319231, -24.63355581998385802, 0.9682620441943947664 ) ) ;
#71417=DIRECTION ( 'NONE',  ( -3.773278334453080206E-23, 0.9999999999976377785, 2.173523156925979975E-06 ) ) ;
#71420=CARTESIAN_POINT ( 'NONE',  ( 8.056674255711671506, 19.11000797562349618, 11.49999999999998934 ) ) ;
#71422=VERTEX_POINT ( 'NONE', #19621 ) ;
#71423=CARTESIAN_POINT ( 'NONE',  ( -89.49044894935767047, -29.50248914370730091, 2.832395270851967073 ) ) ;
#71425=ADVANCED_FACE ( 'NONE', ( #50582 ), #95255, .T. ) ;
#71427=CARTESIAN_POINT ( 'NONE',  ( -108.6228709571500559, -29.50247984919015209, -1.443849546365048253 ) ) ;
#71428=VERTEX_POINT ( 'NONE', #18131 ) ;
#71429=ORIENTED_EDGE ( 'NONE', *, *, #41534, .F. ) ;
#71431=CARTESIAN_POINT ( 'NONE',  ( -40.52287095715006870, -24.52232992886361629, 0.6492154411905992628 ) ) ;
#71432=PLANE ( 'NONE',  #25448 ) ;
#71433=CARTESIAN_POINT ( 'NONE',  ( -28.89873962686151287, -24.82198293592782079, 2.051091576938187444 ) ) ;
#71434=CARTESIAN_POINT ( 'NONE',  ( 13.70243205411677145, -17.22335469805116048, 11.49999999999999645 ) ) ;
#71435=ORIENTED_EDGE ( 'NONE', *, *, #29938, .F. ) ;
#71436=CARTESIAN_POINT ( 'NONE',  ( -101.5895376238167387, -23.47596703998600631, 11.44779298504227683 ) ) ;
#71437=CARTESIAN_POINT ( 'NONE',  ( -13.16310354753345990, -18.33534949228788236, 11.49999999999998934 ) ) ;
#71438=EDGE_CURVE ( 'NONE', #54707, #50701, #89138, .T. ) ;
#71439=CARTESIAN_POINT ( 'NONE',  ( 20.78037738254806399, 3.014218216234254566, 11.49999999999998934 ) ) ;
#71441=CARTESIAN_POINT ( 'NONE',  ( -70.62287095715007013, -24.91544648472620693, 1.928969306349231472 ) ) ;
#71443=B_SPLINE_CURVE_WITH_KNOTS ( 'NONE', 3,
 ( #38380, #99758, #46009, #30263, #16531, #92658 ),
 .UNSPECIFIED., .F., .F.,
 ( 4, 2, 4 ),
 ( 6.391158118975501388E-06, 0.001387004593080791133, 0.002767618028042606766 ),
 .UNSPECIFIED. ) ;
#71451=CARTESIAN_POINT ( 'NONE',  ( 14.48694714638828884, 15.39972936300609341, -1.500000000000002220 ) ) ;
#71452=FACE_OUTER_BOUND ( 'NONE', #94644, .T. ) ;
#71453=CARTESIAN_POINT ( 'NONE',  ( -51.44452858623887437, -25.03148670408844012, 7.233630129720098445 ) ) ;
#71454=CARTESIAN_POINT ( 'NONE',  ( -121.5556940823614127, -23.96119346886880308, -0.6495511937832032512 ) ) ;
#71456=CARTESIAN_POINT ( 'NONE',  ( -47.62287095715004881, -24.64965695001467694, 8.947790433994185832 ) ) ;
#71457=CARTESIAN_POINT ( 'NONE',  ( 19.10802705166043580, 11.29804532628753044, -1.500000000000002220 ) ) ;
#71458=CARTESIAN_POINT ( 'NONE',  ( -74.62287095715005592, -23.47596703998600631, 11.44779298504227860 ) ) ;
#71459=EDGE_CURVE ( 'NONE', #39807, #72214, #95047, .T. ) ;
#71462=CARTESIAN_POINT ( 'NONE',  ( -58.55620429048339304, -23.47596703998600276, 11.44779298504227505 ) ) ;
#71463=CARTESIAN_POINT ( 'NONE',  ( -126.5891258169978784, -24.65952944569305316, 1.056160979905705455 ) ) ;
#71464=FACE_OUTER_BOUND ( 'NONE', #16504, .T. ) ;
#71465=B_SPLINE_CURVE_WITH_KNOTS ( 'NONE', 3,
 ( #52321, #98974, #59945, #60447, #13736, #83753, #75632, #44707, #6133, #99471, #20347, #20850, #37086, #68049, #53323, #45209, #76136, #82261 ),
 .UNSPECIFIED., .F., .F.,
 ( 4, 2, 2, 2, 2, 2, 2, 2, 4 ),
 ( 0.000000000000000000, 0.0002883515756762773229, 0.0005767031513525546459, 0.0008650547270288318604, 0.001153406302705109292, 0.001730109454057662420, 0.002018461029733941044, 0.002162636817572077211, 0.002306812605410212946 ),
 .UNSPECIFIED. ) ;
#71466=CARTESIAN_POINT ( 'NONE',  ( -33.62287095715005592, -23.47596703998600276, 11.44779298504227505 ) ) ;
#71467=EDGE_CURVE ( 'NONE', #17861, #18030, #64844, .T. ) ;
#71468=CARTESIAN_POINT ( 'NONE',  ( -16.97169330436246781, 9.548981535075045102, 11.49999999999998934 ) ) ;
#71469=CARTESIAN_POINT ( 'NONE',  ( 10.55508701655855575, -18.62573008410804221, 11.49999999999998934 ) ) ;
#71472=CARTESIAN_POINT ( 'NONE',  ( -116.6228709571500559, -23.47593901973091235, -1.443836447538997536 ) ) ;
#71473=CARTESIAN_POINT ( 'NONE',  ( -36.92287095715006018, -23.47593901973090169, -1.443836447538998202 ) ) ;
#71474=CARTESIAN_POINT ( 'NONE',  ( -17.66434017299383896, 14.31182286555179139, -1.500000000000002220 ) ) ;
#71475=EDGE_CURVE ( 'NONE', #40343, #61548, #66148, .T. ) ;
#71477=DIRECTION ( 'NONE',  ( 3.773278334444167608E-23, -1.000000000000000000, 0.000000000000000000 ) ) ;
#71479=CARTESIAN_POINT ( 'NONE',  ( -1.214729172165279092, -19.82145330704504360, 11.49999999999999645 ) ) ;
#71483=VERTEX_POINT ( 'NONE', #65829 ) ;
#71484=CARTESIAN_POINT ( 'NONE',  ( -49.27933479010542328, -25.24522353769383898, 6.214461776597443254 ) ) ;
#71486=CARTESIAN_POINT ( 'NONE',  ( -50.89113880358890185, -25.10935775592824726, 2.917241375188960095 ) ) ;
#71487=CARTESIAN_POINT ( 'NONE',  ( -10.04279811845843007, 19.21892966915218892, 11.49999999999998934 ) ) ;
#71488=CARTESIAN_POINT ( 'NONE',  ( -84.52287095715004739, -24.51387760970724372, 9.387446482453409402 ) ) ;
#71489=CARTESIAN_POINT ( 'NONE',  ( 17.91360334016800593, 7.682165803940314674, -1.500000000000002220 ) ) ;
#71490=CARTESIAN_POINT ( 'NONE',  ( -55.52866363368176650, -24.92592662359561118, 8.075495903017996469 ) ) ;
#71492=ORIENTED_EDGE ( 'NONE', *, *, #56419, .T. ) ;
#71493=CARTESIAN_POINT ( 'NONE',  ( 0.5039804632396667206, -20.40334623801319580, 11.49999999999999645 ) ) ;
#71494=DIRECTION ( 'NONE',  ( 0.000000000000000000, -0.9999999999976377785, -2.173523156925979128E-06 ) ) ;
#71496=EDGE_CURVE ( 'NONE', #17763, #100181, #693, .T. ) ;
#71497=CARTESIAN_POINT ( 'NONE',  ( -41.58953762381673158, -23.47593901973091235, -1.443836447539011525 ) ) ;
#71499=CARTESIAN_POINT ( 'NONE',  ( -79.79717327896997858, -25.06342317198667047, 7.417202478348898786 ) ) ;
#71501=CARTESIAN_POINT ( 'NONE',  ( -39.42702772597635175, -25.31628691207657766, 5.331662186571982431 ) ) ;
#71502=CARTESIAN_POINT ( 'NONE',  ( -49.35642674012009223, -25.31439406600090081, 5.792946613328529004 ) ) ;
#71503=CARTESIAN_POINT ( 'NONE',  ( -86.52287095715007581, -23.96127896942158841, -0.6493128930933981247 ) ) ;
#71504=CARTESIAN_POINT ( 'NONE',  ( 13.72940079880349984, -14.68433028913016791, 11.49999999999998934 ) ) ;
#71505=CARTESIAN_POINT ( 'NONE',  ( -87.62287095715004170, -23.47593901973091235, -1.443836447539002865 ) ) ;
#71506=ORIENTED_EDGE ( 'NONE', *, *, #72872, .T. ) ;
#71509=CARTESIAN_POINT ( 'NONE',  ( 22.43992371924722917, 4.826111843257130829, 11.49999999999999645 ) ) ;
#71510=B_SPLINE_CURVE_WITH_KNOTS ( 'NONE', 3,
 ( #10176, #80685, #50247, #63993, #94906, #81184 ),
 .UNSPECIFIED., .F., .F.,
 ( 4, 2, 4 ),
 ( 1.570887131794638196E-05, 0.001396322306279763458, 0.002776935741241580609 ),
 .UNSPECIFIED. ) ;
#71511=CARTESIAN_POINT ( 'NONE',  ( 15.23092229589061830, -16.91372389758942418, 11.49999999999998934 ) ) ;
#71512=VERTEX_POINT ( 'NONE', #84382 ) ;
#71513=CARTESIAN_POINT ( 'NONE',  ( -109.6228709571500417, -24.65952944569305316, 1.056160979905704345 ) ) ;
#71515=CARTESIAN_POINT ( 'NONE',  ( -90.54023547609000389, -25.00158670708910336, 2.256160236439220146 ) ) ;
#71517=CARTESIAN_POINT ( 'NONE',  ( -49.52287095715005449, -23.73907113216989373, -1.053371485793255902 ) ) ;
#71518=CARTESIAN_POINT ( 'NONE',  ( -69.58783992205957247, -24.35071581493542681, 9.817618358456032368 ) ) ;
#71520=CARTESIAN_POINT ( 'NONE',  ( -54.52287095715006160, -23.94994826722564696, -0.6494450866342733608 ) ) ;
#71521=CARTESIAN_POINT ( 'NONE',  ( -58.64320200748918666, -23.96119346886880308, -0.6495511937832116889 ) ) ;
#71523=CARTESIAN_POINT ( 'NONE',  ( -0.5597704280004801580, 20.37679164443051505, 11.49999999999998934 ) ) ;
#71526=CARTESIAN_POINT ( 'NONE',  ( 18.48385363477634513, -13.70420857335572506, 11.49999999999998934 ) ) ;
#71528=VERTEX_POINT ( 'NONE', #90140 ) ;
#71529=DIRECTION ( 'NONE',  ( -3.773278334453079030E-23, 0.9999999999976377785, 2.173523156925979128E-06 ) ) ;
#71530=CARTESIAN_POINT ( 'NONE',  ( -101.5228709571500474, -24.33832256527048088, 0.1851278514138640363 ) ) ;
#71531=CARTESIAN_POINT ( 'NONE',  ( -122.5562042904833930, -24.66019654487199730, 8.947790411086121054 ) ) ;
#71533=CARTESIAN_POINT ( 'NONE',  ( 17.14628872753620215, 12.71262973326862245, 11.49999999999999645 ) ) ;
#71534=ORIENTED_EDGE ( 'NONE', *, *, #2709, .T. ) ;
#71536=CARTESIAN_POINT ( 'NONE',  ( -22.22723998432330106, 0.1330083165726352878, -1.500000000000002220 ) ) ;
#71537=CARTESIAN_POINT ( 'NONE',  ( -15.52656095410427817, -13.64048245868121434, -1.500000000000002220 ) ) ;
#71540=CARTESIAN_POINT ( 'NONE',  ( -95.62721265448736574, -24.73531770709095312, 8.716586749053508498 ) ) ;
#71541=ORIENTED_EDGE ( 'NONE', *, *, #61110, .T. ) ;
#71542=EDGE_CURVE ( 'NONE', #55530, #57540, #100079, .T. ) ;
#71543=DIRECTION ( 'NONE',  ( 0.000000000000000000, 0.9999999999976377785, 2.173523156925979975E-06 ) ) ;
#71544=ORIENTED_EDGE ( 'NONE', *, *, #73377, .F. ) ;
#71545=CARTESIAN_POINT ( 'NONE',  ( -58.61167521426755656, -23.48786465467241058, 11.44779295918254824 ) ) ;
#71548=CARTESIAN_POINT ( 'NONE',  ( 20.83135763335140922, 1.668377004047274959, -1.500000000000002220 ) ) ;
#71549=CARTESIAN_POINT ( 'NONE',  ( -18.37190169643047355, -11.86832528159398237, 11.49999999999999645 ) ) ;
#71550=ADVANCED_FACE ( 'NONE', ( #36355 ), #74414, .F. ) ;
#71551=CARTESIAN_POINT ( 'NONE',  ( -73.58111444669631851, -24.66019654487200441, 8.947790411086119278 ) ) ;
#71552=CARTESIAN_POINT ( 'NONE',  ( -37.62287095715005592, -23.73907113216990439, -1.053371485793235918 ) ) ;
#71553=CARTESIAN_POINT ( 'NONE',  ( -6.794891441663577503, 21.43730618243864683, 11.49999999999998934 ) ) ;
#71554=EDGE_CURVE ( 'NONE', #40469, #50986, #74370, .T. ) ;
#71555=CARTESIAN_POINT ( 'NONE',  ( -44.55620429048339304, -24.64898659630527789, 1.056161002820819039 ) ) ;
#71557=CARTESIAN_POINT ( 'NONE',  ( -78.58953762381673869, -23.48783264082478439, -1.443836473390065711 ) ) ;
#71558=ORIENTED_EDGE ( 'NONE', *, *, #7791, .T. ) ;
#71559=B_SPLINE_CURVE_WITH_KNOTS ( 'NONE', 3,
 ( #46145, #68480, #53262, #29406, #7073, #37027 ),
 .UNSPECIFIED., .F., .F.,
 ( 4, 2, 4 ),
 ( 1.570887131794333942E-05, 0.001396322306279760422, 0.002776935741241577573 ),
 .UNSPECIFIED. ) ;
#71563=CARTESIAN_POINT ( 'NONE',  ( -52.60590739768218782, -23.73766607897671221, -1.055555164236436472 ) ) ;
#71565=CARTESIAN_POINT ( 'NONE',  ( 17.72605931280000391, -11.99821887194124770, -1.500000000000002220 ) ) ;
#71567=CARTESIAN_POINT ( 'NONE',  ( 0.3464652362752086434, -22.36268665536068667, 11.49999999999999645 ) ) ;
#71570=CARTESIAN_POINT ( 'NONE',  ( 21.04674311342985860, -0.3259866984596996864, -1.500000000000002220 ) ) ;
#71571=CARTESIAN_POINT ( 'NONE',  ( -30.57654984345184701, -25.31559415887666020, 6.147639284700202822 ) ) ;
#71572=CARTESIAN_POINT ( 'NONE',  ( 19.80199147212610811, 2.383747631481649254, -1.500000000000002220 ) ) ;
#71573=CARTESIAN_POINT ( 'NONE',  ( -101.5193659238633757, -23.73766607897671221, -1.055555164236452237 ) ) ;
#71574=CARTESIAN_POINT ( 'NONE',  ( -61.52287095715007581, -23.48783264082476308, -1.443836473390092356 ) ) ;
#71575=CARTESIAN_POINT ( 'NONE',  ( -2.902263480631018577, 21.84654903556016947, -1.500000000000002220 ) ) ;
#71576=VERTEX_POINT ( 'NONE', #35853 ) ;
#71577=CARTESIAN_POINT ( 'NONE',  ( -65.49302343295822482, -24.63419186844611275, 9.035850630976918652 ) ) ;
#71579=CARTESIAN_POINT ( 'NONE',  ( -19.85847575633505713, -6.422239212204448044, 11.49999999999999645 ) ) ;
#71581=AXIS2_PLACEMENT_3D ( 'NONE', #60880, #69979, #54273 ) ;
#71582=LINE ( 'NONE', #93392, #5216 ) ;
#71584=CARTESIAN_POINT ( 'NONE',  ( -90.58953762381672448, -25.00158670708909625, 2.256160236439167299 ) ) ;
#71585=CARTESIAN_POINT ( 'NONE',  ( -14.93283513470682067, -15.21490397768744529, -1.500000000000002220 ) ) ;
#71586=CARTESIAN_POINT ( 'NONE',  ( -70.58604916688682351, -25.31487095459964820, 4.870313056136089891 ) ) ;
#71587=CARTESIAN_POINT ( 'NONE',  ( -100.6228709571500559, -29.50250786944525672, 11.44777988621623166 ) ) ;
#71590=CARTESIAN_POINT ( 'NONE',  ( -22.11960324842224423, 4.537628740662121629, -1.500000000000002220 ) ) ;
#71591=PLANE ( 'NONE',  #37685 ) ;
#71592=ORIENTED_EDGE ( 'NONE', *, *, #55903, .F. ) ;
#71593=CARTESIAN_POINT ( 'NONE',  ( -101.6228709571500559, -29.50247984919015209, -1.443849546365050029 ) ) ;
#71594=CARTESIAN_POINT ( 'NONE',  ( -67.92287095715009571, -23.47593901973090524, -1.443836447538997980 ) ) ;
#71595=CARTESIAN_POINT ( 'NONE',  ( 17.62393913918218402, -8.800128315780904487, 11.49999999999999645 ) ) ;
#71598=VERTEX_POINT ( 'NONE', #97748 ) ;
#71600=CARTESIAN_POINT ( 'NONE',  ( -89.52287095715007581, -24.50321055353804667, 9.387540953477524042 ) ) ;
#71601=CARTESIAN_POINT ( 'NONE',  ( -119.5228709571500758, -24.64965694238408034, 8.947790433994191162 ) ) ;
#71603=EDGE_CURVE ( 'NONE', #10167, #27806, #82807, .T. ) ;
#71605=FACE_OUTER_BOUND ( 'NONE', #74143, .T. ) ;
#71606=CARTESIAN_POINT ( 'NONE',  ( 12.99534586470982234, -14.87506298573330632, -1.500000000000002220 ) ) ;
#71607=ORIENTED_EDGE ( 'NONE', *, *, #26300, .F. ) ;
#71608=CARTESIAN_POINT ( 'NONE',  ( -13.58233929615340152, 14.99024694321910900, 11.49999999999999645 ) ) ;
#71609=CARTESIAN_POINT ( 'NONE',  ( -112.6228709571500701, -23.48786465467241769, 11.44779295918254114 ) ) ;
#71610=ADVANCED_FACE ( 'NONE', ( #22958 ), #92985, .F. ) ;
#71611=AXIS2_PLACEMENT_3D ( 'NONE', #97262, #82040, #12519 ) ;
#71613=DIRECTION ( 'NONE',  ( -0.000000000000000000, 2.173523156925979552E-06, -0.9999999999976378895 ) ) ;
#71614=CARTESIAN_POINT ( 'NONE',  ( -69.39786140845737350, -25.27247757640623149, 5.900849392275183902 ) ) ;
#71615=CARTESIAN_POINT ( 'NONE',  ( -100.4498239493576648, -25.26638541557128548, 7.563173708901921088 ) ) ;
#71617=CARTESIAN_POINT ( 'NONE',  ( -62.58953762381672448, -23.48786465467241058, 11.44779295918254824 ) ) ;
#71618=CARTESIAN_POINT ( 'NONE',  ( -86.55620429048337883, -24.66019654487199730, 8.947790411086126383 ) ) ;
#71619=CARTESIAN_POINT ( 'NONE',  ( -19.87929632332335927, 2.386914507623989490, -1.500000000000002220 ) ) ;
#71620=CARTESIAN_POINT ( 'NONE',  ( -99.92788026055190187, -25.10935056794787457, 2.920408329580228557 ) ) ;
#71624=LINE ( 'NONE', #41175, #52616 ) ;
#71625=CARTESIAN_POINT ( 'NONE',  ( -115.6228709571500559, -29.50250786944525672, 11.44777988621622811 ) ) ;
#71629=CARTESIAN_POINT ( 'NONE',  ( -83.63634622578109656, -23.96119346886880308, -0.6495511937832110227 ) ) ;
#71630=DIRECTION ( 'NONE',  ( -3.773278334444167608E-23, 1.000000000000000000, 0.000000000000000000 ) ) ;
#71631=DIRECTION ( 'NONE',  ( 0.000000000000000000, -2.173523156925980399E-06, 0.9999999999976378895 ) ) ;
#71632=ORIENTED_EDGE ( 'NONE', *, *, #72010, .F. ) ;
#71633=CARTESIAN_POINT ( 'NONE',  ( 5.347689060783223702, 19.56899250667117229, 11.49999999999998934 ) ) ;
#71636=CARTESIAN_POINT ( 'NONE',  ( -59.49368872175574552, -24.51419770103156281, 9.386484678747184063 ) ) ;
#71638=EDGE_CURVE ( 'NONE', #82766, #7634, #43966, .T. ) ;
#71640=B_SPLINE_CURVE_WITH_KNOTS ( 'NONE', 3,
 ( #51485, #51984, #13899, #43870 ),
 .UNSPECIFIED., .F., .F.,
 ( 4, 4 ),
 ( 0.000000000000000000, 9.999999999998206125E-05 ),
 .UNSPECIFIED. ) ;
#71642=CARTESIAN_POINT ( 'NONE',  ( 13.25904570721172604, 16.46799385432867169, 11.49999999999999645 ) ) ;
#71644=CARTESIAN_POINT ( 'NONE',  ( -21.88945651911318535, 3.243594245096953710, 11.49999999999998934 ) ) ;
#71645=CARTESIAN_POINT ( 'NONE',  ( 3.262959013008915665, -20.29835246810489835, 11.49999999999998934 ) ) ;
#71646=ORIENTED_EDGE ( 'NONE', *, *, #47477, .F. ) ;
#71650=CARTESIAN_POINT ( 'NONE',  ( -68.62287095715005592, -29.50247984919015209, -1.443849546365055359 ) ) ;
#71652=ADVANCED_FACE ( 'NONE', ( #7758 ), #66900, .T. ) ;
#71653=VERTEX_POINT ( 'NONE', #20258 ) ;
#71655=CARTESIAN_POINT ( 'NONE',  ( -100.5228709571500758, -24.51163499207175533, 0.6490370598554370263 ) ) ;
#71656=B_SPLINE_CURVE_WITH_KNOTS ( 'NONE', 3,
 ( #6006, #87870, #41712, #64560 ),
 .UNSPECIFIED., .F., .F.,
 ( 4, 4 ),
 ( 0.8293726295494769918, 0.8303733765902421293 ),
 .UNSPECIFIED. ) ;
#71658=CARTESIAN_POINT ( 'NONE',  ( -91.62287095715004170, -23.96127896941631619, -0.6493128931037837059 ) ) ;
#71659=CARTESIAN_POINT ( 'NONE',  ( 9.361532043782798240, 18.45020211870636118, -1.500000000000002220 ) ) ;
#71660=CARTESIAN_POINT ( 'NONE',  ( 13.31326451270642330, 17.06472021985377552, 11.49999999999999645 ) ) ;
#71661=ORIENTED_EDGE ( 'NONE', *, *, #14952, .T. ) ;
#71663=CARTESIAN_POINT ( 'NONE',  ( -98.89303308397303738, -25.25494757631710385, 6.110950176066591411 ) ) ;
#71665=CARTESIAN_POINT ( 'NONE',  ( 1.926536275058113867, -22.33200895297504474, 11.49999999999998934 ) ) ;
#71667=CARTESIAN_POINT ( 'NONE',  ( -79.47715298469661604, -25.27874961927179953, 6.508607590754126093 ) ) ;
#71668=DIRECTION ( 'NONE',  ( 0.000000000000000000, -0.9999999999976377785, -2.173523156925979128E-06 ) ) ;
#71669=ORIENTED_EDGE ( 'NONE', *, *, #50774, .F. ) ;
#71671=LINE ( 'NONE', #93482, #62050 ) ;
#71672=EDGE_CURVE ( 'NONE', #59761, #58570, #10216, .T. ) ;
#71673=ORIENTED_EDGE ( 'NONE', *, *, #90091, .T. ) ;
#71674=EDGE_CURVE ( 'NONE', #49847, #26695, #54969, .T. ) ;
#71676=CARTESIAN_POINT ( 'NONE',  ( -109.6228709571500559, -23.47596703998600631, 11.44779298504227860 ) ) ;
#71679=CARTESIAN_POINT ( 'NONE',  ( -6.347832186973104029, -20.24257907634199682, -1.500000000000002220 ) ) ;
#71681=FACE_OUTER_BOUND ( 'NONE', #75392, .T. ) ;
#71683=CARTESIAN_POINT ( 'NONE',  ( -21.01659442711627790, -5.882202039844940167, 11.49999999999998934 ) ) ;
#71684=CARTESIAN_POINT ( 'NONE',  ( -52.58235619518457327, -24.51419770103158413, 9.386484678747189392 ) ) ;
#71685=CARTESIAN_POINT ( 'NONE',  ( -107.5228709571500758, -24.64898659630367916, 1.056161002820831474 ) ) ;
#71686=CARTESIAN_POINT ( 'NONE',  ( -35.52287095715006870, -23.47596703998600631, 11.44779298504229281 ) ) ;
#71687=CARTESIAN_POINT ( 'NONE',  ( 19.20967809413044236, -10.42350525531561978, -1.500000000000002220 ) ) ;
#71688=CARTESIAN_POINT ( 'NONE',  ( -30.57287095715007652, -24.67296300714258805, 8.878589634568275102 ) ) ;
#71690=EDGE_CURVE ( 'NONE', #41555, #21327, #1778, .T. ) ;
#71692=CARTESIAN_POINT ( 'NONE',  ( -85.54469269819122701, -24.63419186844611275, 9.035850630976915099 ) ) ;
#71693=ORIENTED_EDGE ( 'NONE', *, *, #80182, .T. ) ;
#71695=VERTEX_POINT ( 'NONE', #72571 ) ;
#71696=VECTOR ( 'NONE', #26792, 1000.000000000000114 ) ;
#71697=LINE ( 'NONE', #31115, #52442 ) ;
#71699=CARTESIAN_POINT ( 'NONE',  ( -14.73150212448299357, 15.28860238833873808, 11.49999999999998934 ) ) ;
#71702=CARTESIAN_POINT ( 'NONE',  ( -41.62287095715006302, -24.65952944569303895, 1.056160979905692576 ) ) ;
#71704=PLANE ( 'NONE',  #54062 ) ;
#71705=CARTESIAN_POINT ( 'NONE',  ( -1.428710472040144452, 19.32843595812722626, -1.500000000000002220 ) ) ;
#71706=CARTESIAN_POINT ( 'NONE',  ( -117.5877651003913229, -24.66019654487200441, 8.947790411086110396 ) ) ;
#71707=ORIENTED_EDGE ( 'NONE', *, *, #59236, .T. ) ;
#71708=CARTESIAN_POINT ( 'NONE',  ( 18.70946937610417038, -5.484834493922766896, 11.49999999999999645 ) ) ;
#71714=CARTESIAN_POINT ( 'NONE',  ( -119.5895376238167103, -24.64965694238408034, 8.947790433994649462 ) ) ;
#71719=CARTESIAN_POINT ( 'NONE',  ( -17.62575346185542102, 8.740161020289619387, -1.500000000000002220 ) ) ;
#71721=EDGE_LOOP ( 'NONE', ( #73687, #43188, #43469, #91047 ) ) ;
#71723=CARTESIAN_POINT ( 'NONE',  ( -100.6228709571500559, -29.50248789122583659, 2.256150453626215580 ) ) ;
#71724=VECTOR ( 'NONE', #13655, 1000.000000000000114 ) ;
#71726=ADVANCED_FACE ( 'NONE', ( #51226 ), #82170, .F. ) ;
#71728=CARTESIAN_POINT ( 'NONE',  ( -90.52287095715006160, -23.47596703998600631, 11.44779298504228393 ) ) ;
#71729=CARTESIAN_POINT ( 'NONE',  ( -114.5228709571500616, -24.64898659630529565, 1.056161002820831474 ) ) ;
#71730=CARTESIAN_POINT ( 'NONE',  ( -76.52287095715006160, -24.51283580621364067, 0.6167428607019798115 ) ) ;
#71731=CARTESIAN_POINT ( 'NONE',  ( -80.91469753264981080, -25.03722721891040948, 7.590183713343859218 ) ) ;
#71732=CARTESIAN_POINT ( 'NONE',  ( -50.40445135320379677, -25.19502912051677868, 3.293943094755626078 ) ) ;
#71733=CARTESIAN_POINT ( 'NONE',  ( -121.6228709571500275, -23.73934037231757799, 11.05740245334328087 ) ) ;
#71735=CARTESIAN_POINT ( 'NONE',  ( -78.62287095715005592, -29.50250243563736774, 8.947779886222141599 ) ) ;
#71736=CARTESIAN_POINT ( 'NONE',  ( -19.52388446859773552, -3.948942086532154061, 11.49999999999998934 ) ) ;
#71737=EDGE_CURVE ( 'NONE', #79772, #37238, #21254, .T. ) ;
#71738=CARTESIAN_POINT ( 'NONE',  ( -75.49987233357580863, -24.52399227489127043, 9.353111116836526406 ) ) ;
#71739=CARTESIAN_POINT ( 'NONE',  ( 15.03354914759215966, -12.96403794047452607, -1.500000000000002220 ) ) ;
#71740=ORIENTED_EDGE ( 'NONE', *, *, #87111, .F. ) ;
#71742=CARTESIAN_POINT ( 'NONE',  ( -51.52764846858840997, -25.25773520710183817, 6.187572766161611781 ) ) ;
#71744=CARTESIAN_POINT ( 'NONE',  ( -19.11632921840048738, -8.121837694355717119, 11.49999999999999645 ) ) ;
#71747=CARTESIAN_POINT ( 'NONE',  ( -56.62287095715005592, -24.65952944569304250, 1.056160979905693464 ) ) ;
#71748=CARTESIAN_POINT ( 'NONE',  ( -17.51746294255814718, -14.55262482891283504, 11.49999999999999645 ) ) ;
#71750=VERTEX_POINT ( 'NONE', #99382 ) ;
#71751=B_SPLINE_SURFACE_WITH_KNOTS ( 'NONE', 3, 3, ( 
 ( #94879, #4047, #48734, #25371 ),
 ( #79653, #71563, #3550, #19253 ),
 ( #34989, #49733, #10152, #72069 ),
 ( #2550, #3054, #42124, #33484 ),
 ( #56350, #87269, #49236, #80165 ),
 ( #81163, #72559, #33995, #26878 ),
 ( #64972, #50720, #26380, #57350 ) ),
 .UNSPECIFIED., .F., .F., .F.,
 ( 4, 3, 4 ),
 ( 4, 4 ),
 ( 0.0004766839783839493675, 0.1029713700210903582, 0.2054660560637967537 ),
 ( 0.7796923376582600707, 0.7810648108262568945 ),
 .UNSPECIFIED. ) ;
#71752=CARTESIAN_POINT ( 'NONE',  ( -111.6228709571500843, -23.47596703998600631, 11.44779298504227860 ) ) ;
#71753=CARTESIAN_POINT ( 'NONE',  ( -90.92287095715006728, -23.47596703998600631, 11.44779298504227860 ) ) ;
#71755=CARTESIAN_POINT ( 'NONE',  ( -20.01257119864951051, 2.908879540851186274, -1.500000000000002220 ) ) ;
#71757=CARTESIAN_POINT ( 'NONE',  ( -97.62287095715002749, -23.72773821059535848, 11.05748984161097503 ) ) ;
#71758=AXIS2_PLACEMENT_3D ( 'NONE', #33706, #40811, #25586 ) ;
#71762=CARTESIAN_POINT ( 'NONE',  ( -11.57650325489309395, -16.32560983125179277, -1.500000000000002220 ) ) ;
#71765=CARTESIAN_POINT ( 'NONE',  ( 5.463070048063013218, -20.23478146675526190, 11.49999999999999645 ) ) ;
#71766=CARTESIAN_POINT ( 'NONE',  ( -29.78625860165176320, -25.23684457897835287, 5.682942667385789903 ) ) ;
#71767=CARTESIAN_POINT ( 'NONE',  ( -124.6228709571500417, -23.95044443724992433, 10.65354141964649415 ) ) ;
#71768=CARTESIAN_POINT ( 'NONE',  ( 4.500060333422437608, -21.59917750860068963, 11.49999999999998934 ) ) ;
#71771=CARTESIAN_POINT ( 'NONE',  ( -26.09636659181000695, -24.95932275238217102, 4.940287574183225061 ) ) ;
#71773=CARTESIAN_POINT ( 'NONE',  ( -50.62287095715005592, -24.99132157543083821, 2.256160258750667502 ) ) ;
#71774=EDGE_LOOP ( 'NONE', ( #38392, #81902, #10608, #73197 ) ) ;
#71776=B_SPLINE_CURVE_WITH_KNOTS ( 'NONE', 3,
 ( #22401, #38640, #46260, #68601, #31529, #77189 ),
 .UNSPECIFIED., .F., .F.,
 ( 4, 2, 4 ),
 ( 1.570887131794638196E-05, 0.001396322306279759555, 0.002776935741241572803 ),
 .UNSPECIFIED. ) ;
#71777=ORIENTED_EDGE ( 'NONE', *, *, #73316, .T. ) ;
#71778=ORIENTED_EDGE ( 'NONE', *, *, #71798, .T. ) ;
#71779=EDGE_CURVE ( 'NONE', #32503, #79100, #91264, .T. ) ;
#71781=CARTESIAN_POINT ( 'NONE',  ( -101.1996739087839075, -25.10935851964410759, 3.060140785615252046 ) ) ;
#71783=CARTESIAN_POINT ( 'NONE',  ( 9.245221688665949955, -18.36014492602614467, -1.500000000000002220 ) ) ;
#71784=ORIENTED_EDGE ( 'NONE', *, *, #59512, .F. ) ;
#71785=CARTESIAN_POINT ( 'NONE',  ( -100.3681461616303636, -25.30369546473245634, 5.218539490501125755 ) ) ;
#71788=CARTESIAN_POINT ( 'NONE',  ( -22.28969446433750434, -1.297463027894488086, 11.49999999999998934 ) ) ;
#71790=CARTESIAN_POINT ( 'NONE',  ( -0.05748996396964648620, -22.30574723846597962, 8.909134979017297340 ) ) ;
#71792=ORIENTED_EDGE ( 'NONE', *, *, #53122, .T. ) ;
#71797=CARTESIAN_POINT ( 'NONE',  ( -6.911038104174170194, -19.68591361114308214, 11.49999999999998934 ) ) ;
#71798=EDGE_CURVE ( 'NONE', #34509, #79503, #50124, .T. ) ;
#71800=CARTESIAN_POINT ( 'NONE',  ( -116.5228709571499905, -23.48783264083416711, -1.443836473375476270 ) ) ;
#71801=VERTEX_POINT ( 'NONE', #90285 ) ;
#71802=EDGE_LOOP ( 'NONE', ( #87971, #80260, #78399, #20339 ) ) ;
#71805=CARTESIAN_POINT ( 'NONE',  ( 16.43158684610488862, 13.14696595092960152, -1.500000000000002220 ) ) ;
#71807=CARTESIAN_POINT ( 'NONE',  ( -69.52287095715003318, -24.66019654487199375, 8.947790411086119278 ) ) ;
#71809=CARTESIAN_POINT ( 'NONE',  ( -120.5520467162983067, -25.00182538069147142, 7.747789668545046027 ) ) ;
#71810=VECTOR ( 'NONE', #95251, 1000.000000000000114 ) ;
#71811=CARTESIAN_POINT ( 'NONE',  ( -86.55835959473523644, -23.73791477778911840, 11.05961554403170766 ) ) ;
#71812=CARTESIAN_POINT ( 'NONE',  ( -59.53837624874798706, -24.51314013834316441, 0.6176544820404136216 ) ) ;
#71813=CARTESIAN_POINT ( 'NONE',  ( 21.21565077533257337, 4.556159429511043690, -1.500000000000002220 ) ) ;
#71814=CARTESIAN_POINT ( 'NONE',  ( -63.55620429048339304, -24.64898659630528144, 1.056161002820822370 ) ) ;
#71815=CARTESIAN_POINT ( 'NONE',  ( 21.95989154999629278, -3.605859658025859282, 11.49999999999999645 ) ) ;
#71818=CARTESIAN_POINT ( 'NONE',  ( -51.02375840103924531, -25.31441758376955065, 5.363929648462054445 ) ) ;
#71819=CARTESIAN_POINT ( 'NONE',  ( -69.52287095715006160, -23.48786465467241058, 11.44779295918254647 ) ) ;
#71821=CARTESIAN_POINT ( 'NONE',  ( 4.697487806458584991, -22.17256498326293013, 11.49999999999998934 ) ) ;
#71824=ORIENTED_EDGE ( 'NONE', *, *, #4444, .T. ) ;
#71826=CARTESIAN_POINT ( 'NONE',  ( 17.11712468798820908, 10.61635618877791742, -1.500000000000002220 ) ) ;
#71827=CARTESIAN_POINT ( 'NONE',  ( -36.62287095715005592, -24.66019654487199020, 8.947790411086138818 ) ) ;
#71828=ORIENTED_EDGE ( 'NONE', *, *, #68252, .F. ) ;
#71829=CARTESIAN_POINT ( 'NONE',  ( -130.5728709571500588, -24.90664209387383110, 1.540770492762566057 ) ) ;
#71830=CARTESIAN_POINT ( 'NONE',  ( -16.61153998044026991, -15.06042057022924929, -1.500000000000002220 ) ) ;
#71831=ORIENTED_EDGE ( 'NONE', *, *, #44099, .T. ) ;
#71832=VERTEX_POINT ( 'NONE', #29376 ) ;
#71835=CARTESIAN_POINT ( 'NONE',  ( -101.5105846445331679, -24.51419770103158413, 9.386484678747175181 ) ) ;
#71836=CARTESIAN_POINT ( 'NONE',  ( -39.78092239315489564, -25.31507905443482542, 4.883898260817319148 ) ) ;
#71837=DIRECTION ( 'NONE',  ( -3.773278334453079030E-23, 0.9999999999976377785, 2.173523156925979128E-06 ) ) ;
#71838=CARTESIAN_POINT ( 'NONE',  ( -30.60524947077498936, -24.47827083238275492, 0.5637492489085982328 ) ) ;
#71839=EDGE_CURVE ( 'NONE', #79516, #11582, #69524, .T. ) ;
#71840=CARTESIAN_POINT ( 'NONE',  ( -19.30006219055749739, -3.230038287793697283, -1.500000000000002220 ) ) ;
#71841=AXIS2_PLACEMENT_3D ( 'NONE', #21420, #28546, #59515 ) ;
#71842=CARTESIAN_POINT ( 'NONE',  ( -46.50655037741685760, -23.96119346886880308, -0.6495511937832144644 ) ) ;
#71844=CARTESIAN_POINT ( 'NONE',  ( 20.53733210929814845, -6.371126427052321795, 11.49999999999998934 ) ) ;
#71845=CARTESIAN_POINT ( 'NONE',  ( -128.5903318345393984, -23.48783264082479150, -1.443836473390056829 ) ) ;
#71847=CARTESIAN_POINT ( 'NONE',  ( -51.93149462243456327, -25.24900417239232908, 6.174051150523328424 ) ) ;
#71848=CARTESIAN_POINT ( 'NONE',  ( -77.62287095715007013, -24.35013146730204525, 9.818937971375111928 ) ) ;
#71849=CARTESIAN_POINT ( 'NONE',  ( -22.60589916338503613, 3.847557683979087706, -1.500000000000002220 ) ) ;
#71850=EDGE_CURVE ( 'NONE', #39979, #11739, #53731, .T. ) ;
#71851=ADVANCED_FACE ( 'NONE', ( #22248 ), #91279, .F. ) ;
#71853=DIRECTION ( 'NONE',  ( 0.000000000000000000, -0.9999999999976377785, -2.173523156925979128E-06 ) ) ;
#71854=CARTESIAN_POINT ( 'NONE',  ( -42.52287095715005449, -24.65952944569303895, 1.056160979905691910 ) ) ;
#71855=CARTESIAN_POINT ( 'NONE',  ( -18.49208213979201076, -7.923680710433813168, 11.49999999999999645 ) ) ;
#71856=CARTESIAN_POINT ( 'NONE',  ( -110.2646033073992129, -25.10927396522695432, 2.833559977893872261 ) ) ;
#71857=LINE ( 'NONE', #80458, #63071 ) ;
#71858=CARTESIAN_POINT ( 'NONE',  ( -99.52287095715006160, -24.65952944569304961, 1.056160979905702346 ) ) ;
#71859=CARTESIAN_POINT ( 'NONE',  ( -38.55620429048339304, -24.64965694238574656, 8.947790433994203596 ) ) ;
#71861=CARTESIAN_POINT ( 'NONE',  ( 13.50462702941046977, 14.53317887778067252, -1.500000000000002220 ) ) ;
#71862=CARTESIAN_POINT ( 'NONE',  ( 17.47290450027814757, -12.96279059203284767, 11.49999999999998934 ) ) ;
#71863=CARTESIAN_POINT ( 'NONE',  ( -90.62287095715009855, -24.52323809116983355, 9.355190652339423707 ) ) ;
#71864=CARTESIAN_POINT ( 'NONE',  ( 10.71975780190685690, -16.47196428025586812, -1.500000000000002220 ) ) ;
#71865=CARTESIAN_POINT ( 'NONE',  ( -42.64758970778231628, -23.96119346886880663, -0.6495511937831991434 ) ) ;
#71867=LINE ( 'NONE', #94685, #64598 ) ;
#71870=CARTESIAN_POINT ( 'NONE',  ( 3.262959013008915665, -20.29835246810489835, 11.49999999999999645 ) ) ;
#71872=EDGE_CURVE ( 'NONE', #81148, #20503, #70790, .T. ) ;
#71873=CARTESIAN_POINT ( 'NONE',  ( -42.62287095715004881, -24.65952944569303895, 1.056160979905691688 ) ) ;
#71876=CARTESIAN_POINT ( 'NONE',  ( -22.13905560727926414, 4.690293145198261904, 11.49999999999999645 ) ) ;
#71877=ORIENTED_EDGE ( 'NONE', *, *, #69043, .F. ) ;
#71879=CARTESIAN_POINT ( 'NONE',  ( -31.62287095715005236, -29.50250786944525672, 11.44777988621624409 ) ) ;
#71880=CARTESIAN_POINT ( 'NONE',  ( -109.6228709571500701, -23.72773821059536559, 11.05748984161097503 ) ) ;
#71883=CARTESIAN_POINT ( 'NONE',  ( -110.6228709571500417, -23.84081130438200802, 10.88220057463248835 ) ) ;
#71884=CARTESIAN_POINT ( 'NONE',  ( -28.52287095715006870, -24.18853882557989010, 9.819127037903783162 ) ) ;
#71885=EDGE_CURVE ( 'NONE', #4386, #98717, #38988, .T. ) ;
#71887=ORIENTED_EDGE ( 'NONE', *, *, #58902, .T. ) ;
#71888=CARTESIAN_POINT ( 'NONE',  ( 20.31487730549432413, -11.01532776123576518, 11.49999999999999645 ) ) ;
#71889=CARTESIAN_POINT ( 'NONE',  ( -10.82450569625279613, 20.10975305113172951, -1.500000000000002220 ) ) ;
#71890=CARTESIAN_POINT ( 'NONE',  ( -110.9788531467586381, -25.21179375825580493, 3.492134297454125846 ) ) ;
#71892=CARTESIAN_POINT ( 'NONE',  ( -63.59272554027524649, -24.15620529776628089, 10.23563542870660470 ) ) ;
#71893=CARTESIAN_POINT ( 'NONE',  ( -22.46026885398333661, -0.8929446408661095846, 11.49999999999999645 ) ) ;
#71894=ORIENTED_EDGE ( 'NONE', *, *, #96979, .F. ) ;
#71896=CARTESIAN_POINT ( 'NONE',  ( -21.97012646571106842, -0.5360883523215664859, -1.500000000000002220 ) ) ;
#71898=CARTESIAN_POINT ( 'NONE',  ( -126.3656671591979688, -25.31826104724057913, 3.540018580561483663 ) ) ;
#71899=FACE_OUTER_BOUND ( 'NONE', #49988, .T. ) ;
#71901=VERTEX_POINT ( 'NONE', #85160 ) ;
#71902=DIRECTION ( 'NONE',  ( 0.000000000000000000, 0.9999999999976377785, 2.173523156925979128E-06 ) ) ;
#71903=LINE ( 'NONE', #97227, #73775 ) ;
#71905=CARTESIAN_POINT ( 'NONE',  ( 10.70087849588422380, -17.49211976490306597, 11.49999999999998934 ) ) ;
#71909=ORIENTED_EDGE ( 'NONE', *, *, #66447, .F. ) ;
#71911=EDGE_CURVE ( 'NONE', #72639, #42765, #6615, .T. ) ;
#71913=CARTESIAN_POINT ( 'NONE',  ( 21.75596283627254479, -7.788036635067100200, 11.49999999999998934 ) ) ;
#71914=CARTESIAN_POINT ( 'NONE',  ( -63.62287095715007723, -23.47596703998600631, 11.44779298504227683 ) ) ;
#71915=CARTESIAN_POINT ( 'NONE',  ( 17.42226438573850800, -10.51879874471254261, -1.500000000000002220 ) ) ;
#71918=PLANE ( 'NONE',  #93100 ) ;
#71919=CARTESIAN_POINT ( 'NONE',  ( -29.52490032455085611, -24.57700738376806626, 8.947790440257527678 ) ) ;
#71922=CARTESIAN_POINT ( 'NONE',  ( 7.253797376210795456, 20.28272692992397808, 11.49999999999999645 ) ) ;
#71924=CARTESIAN_POINT ( 'NONE',  ( -29.17364183714287762, -24.76881193471582066, 3.835941365018065596 ) ) ;
#71925=FACE_OUTER_BOUND ( 'NONE', #59801, .T. ) ;
#71928=CARTESIAN_POINT ( 'NONE',  ( -12.26507114386991226, -16.75673120704366426, -1.500000000000002220 ) ) ;
#71930=ORIENTED_EDGE ( 'NONE', *, *, #43418, .F. ) ;
#71931=CARTESIAN_POINT ( 'NONE',  ( -125.5204591733787822, -24.40034930558991633, 0.3402023900116222244 ) ) ;
#71936=ORIENTED_EDGE ( 'NONE', *, *, #62784, .F. ) ;
#71938=FACE_OUTER_BOUND ( 'NONE', #23761, .T. ) ;
#71940=CARTESIAN_POINT ( 'NONE',  ( -29.80801515927848655, -25.24993384078980085, 4.570450481866611625 ) ) ;
#71941=CARTESIAN_POINT ( 'NONE',  ( 15.63414672909509839, 15.54323407889855879, 11.49999999999999645 ) ) ;
#71943=EDGE_CURVE ( 'NONE', #47459, #49734, #52634, .T. ) ;
#71945=CARTESIAN_POINT ( 'NONE',  ( -3.174168706971715270, 22.36591850054903929, -1.500000000000002220 ) ) ;
#71946=EDGE_CURVE ( 'NONE', #51976, #41756, #75608, .T. ) ;
#71947=CARTESIAN_POINT ( 'NONE',  ( -79.73149462243461016, -25.13069340115296058, 2.947789388436138580 ) ) ;
#71948=EDGE_LOOP ( 'NONE', ( #59799, #61415, #86615, #34360, #49690 ) ) ;
#71949=EDGE_LOOP ( 'NONE', ( #23442, #32891, #9092, #34844 ) ) ;
#71950=CARTESIAN_POINT ( 'NONE',  ( -72.62287095715005592, -29.50250243563736774, 8.947779886222143375 ) ) ;
#71952=CARTESIAN_POINT ( 'NONE',  ( -46.52287095715006160, -29.50247984919015209, -1.443849546365058689 ) ) ;
#71954=CARTESIAN_POINT ( 'NONE',  ( 21.03498508994548999, -2.205306954651367946, -1.500000000000002220 ) ) ;
#71955=CARTESIAN_POINT ( 'NONE',  ( -34.62287095715005592, -24.35013146730203459, 9.818937971375117257 ) ) ;
#71956=CARTESIAN_POINT ( 'NONE',  ( -61.66125566941204994, -25.29489609436098263, 6.057563354383567855 ) ) ;
#71958=CARTESIAN_POINT ( 'NONE',  ( -80.62287095715008434, -24.52323809116982289, 9.355190652339425483 ) ) ;
#71959=CARTESIAN_POINT ( 'NONE',  ( -13.35739915041183323, 17.77566839534079435, -1.500000000000002220 ) ) ;
#71961=PLANE ( 'NONE',  #38666 ) ;
#71962=ORIENTED_EDGE ( 'NONE', *, *, #100154, .T. ) ;
#71965=CARTESIAN_POINT ( 'NONE',  ( -17.77321681866180469, -7.816401696202086136, 11.49999999999999645 ) ) ;
#71966=CARTESIAN_POINT ( 'NONE',  ( -36.49753981958003379, -24.15620529776627379, 10.23563542870660825 ) ) ;
#71969=CARTESIAN_POINT ( 'NONE',  ( -10.96721834449554933, 16.09610527815933168, -1.500000000000002220 ) ) ;
#71970=CARTESIAN_POINT ( 'NONE',  ( 9.091334071971768793, -19.38302982324925239, 11.49999999999998934 ) ) ;
#71971=CARTESIAN_POINT ( 'NONE',  ( -32.62287095715004881, -24.64965695001467694, 8.947790433994189385 ) ) ;
#71972=DIRECTION ( 'NONE',  ( 3.773278334444167608E-23, -1.000000000000000000, 0.000000000000000000 ) ) ;
#71973=CARTESIAN_POINT ( 'NONE',  ( -51.63915335351398994, -24.15543982623907127, -0.2315651400026664530 ) ) ;
#71974=CARTESIAN_POINT ( 'NONE',  ( -52.62287095715005592, -23.48786465467240703, 11.44779295918255002 ) ) ;
#71975=CARTESIAN_POINT ( 'NONE',  ( -20.44213351528904354, 10.05872170072450977, -1.500000000000002220 ) ) ;
#71977=CARTESIAN_POINT ( 'NONE',  ( -106.5125960639114027, -24.51419770103158768, 9.386484678747164523 ) ) ;
#71979=CARTESIAN_POINT ( 'NONE',  ( 12.81631318294326505, -15.22695477405695996, 11.49999999999999645 ) ) ;
#71980=CARTESIAN_POINT ( 'NONE',  ( -123.6253775573720475, -23.96169478059714919, 10.65365249895717348 ) ) ;
#71982=CARTESIAN_POINT ( 'NONE',  ( -128.5228709571500758, -23.47596703998600631, 11.44779298504227683 ) ) ;
#71983=DIRECTION ( 'NONE',  ( -3.773278334453080206E-23, 0.9999999999976377785, 2.173523156925979975E-06 ) ) ;
#71984=ORIENTED_EDGE ( 'NONE', *, *, #75688, .F. ) ;
#71986=CARTESIAN_POINT ( 'NONE',  ( -32.99704036429253762, -25.31558585043574183, 4.997857581739419075 ) ) ;
#71987=B_SPLINE_CURVE_WITH_KNOTS ( 'NONE', 3,
 ( #83923, #4317, #75802, #20030, #5302, #50995 ),
 .UNSPECIFIED., .F., .F.,
 ( 4, 2, 4 ),
 ( 0.000000000000000000, 0.001380764517854763014, 0.002761529035709526028 ),
 .UNSPECIFIED. ) ;
#71989=DIRECTION ( 'NONE',  ( 1.000000000000000000, 3.773278334444167608E-23, 8.201307833595939069E-29 ) ) ;
#71990=CARTESIAN_POINT ( 'NONE',  ( 9.217229664113554932, 19.63635308506117383, -1.500000000000002220 ) ) ;
#71991=CARTESIAN_POINT ( 'NONE',  ( -51.72093146136422348, -25.16667630403369671, 6.901880236027385429 ) ) ;
#71992=CARTESIAN_POINT ( 'NONE',  ( 5.544562197198338538, -18.70016399976332977, -1.500000000000002220 ) ) ;
#71995=AXIS2_PLACEMENT_3D ( 'NONE', #29574, #45805, #14338 ) ;
#71996=CARTESIAN_POINT ( 'NONE',  ( -14.54385459823299875, 14.27422344363935025, 11.49999999999999645 ) ) ;
#71997=CARTESIAN_POINT ( 'NONE',  ( -49.58953762381671737, -23.47596703998600276, 11.44779298504227505 ) ) ;
#72000=ORIENTED_EDGE ( 'NONE', *, *, #79118, .F. ) ;
#72001=CARTESIAN_POINT ( 'NONE',  ( -0.07965933291641426328, -22.01874733586428690, 9.960208392924579712 ) ) ;
#72004=CARTESIAN_POINT ( 'NONE',  ( -125.5562042904833646, -23.48786465467241413, 11.44779295918253581 ) ) ;
#72007=ORIENTED_EDGE ( 'NONE', *, *, #11318, .F. ) ;
#72008=EDGE_CURVE ( 'NONE', #20514, #31485, #36814, .T. ) ;
#72010=EDGE_CURVE ( 'NONE', #73650, #62726, #48118, .T. ) ;
#72012=CARTESIAN_POINT ( 'NONE',  ( -21.13427563780003382, 8.902639844219676135, 11.49999999999999645 ) ) ;
#72013=CARTESIAN_POINT ( 'NONE',  ( 21.73672277138745201, -6.736064506363727666, -1.500000000000002220 ) ) ;
#72014=CARTESIAN_POINT ( 'NONE',  ( -71.54080034593859239, -25.17052887806732997, 6.883280112116211491 ) ) ;
#72015=CARTESIAN_POINT ( 'NONE',  ( -77.62287095715005592, -29.50247984919015209, -1.443849546365053582 ) ) ;
#72016=CARTESIAN_POINT ( 'NONE',  ( -90.54280940977186276, -24.83618233451451118, 1.606449574219535492 ) ) ;
#72018=CARTESIAN_POINT ( 'NONE',  ( -69.39514063290955903, -25.22191518979476754, 6.510382875654499912 ) ) ;
#72019=CARTESIAN_POINT ( 'NONE',  ( -6.606886629844116676, -20.84447163495035937, -1.500000000000002220 ) ) ;
#72020=CARTESIAN_POINT ( 'NONE',  ( -69.59245699313737532, -24.15620529776627734, 10.23563542870660825 ) ) ;
#72023=CARTESIAN_POINT ( 'NONE',  ( -40.22287095715007155, -23.47593901973090169, -1.443836447538997980 ) ) ;
#72024=ORIENTED_EDGE ( 'NONE', *, *, #3859, .T. ) ;
#72025=CARTESIAN_POINT ( 'NONE',  ( -18.16121111207539940, 9.348575961806686152, 11.49999999999998934 ) ) ;
#72026=EDGE_LOOP ( 'NONE', ( #38467, #12329, #14450, #36914, #59222, #77967, #53478, #11519, #95612, #62042, #21453, #58002, #12699, #15477, #88612, #16439, #1992, #3376, #11753, #67608, #36835, #39950, #71777, #46119, #60711, #64018, #75037, #92824, #40214, #3161, #86884, #516, #35518, #98459, #54257, #66845, #77507, #3188, #11022, #9214, #68649, #21885, #7682, #38091, #68564, #42395, #41831, #37330, #1303, #14094, #30726, #99417, #172, #31741, #86233, #6104, #42579, #60325, #99258, #86642, #3790, #37847, #7620, #26833, #16571, #62078, #94352, #60932, #47153, #70149, #88618, #80802, #65390, #76899, #97125, #65336, #85902, #52254, #51330, #71009, #41941, #80422, #17352, #36615, #33991, #45380, #12121, #89379, #77621, #35595, #61021, #78530, #9992, #27615, #70671, #61196, #60461, #64591, #6267, #26356, #12964, #4393, #76110, #39089, #26136, #82002, #63520, #15964, #2088, #6532, #277, #49584, #17411, #100265, #57967, #55681, #47798, #62661, #97346, #80277, #298, #58012, #10031, #15783, #52268, #49380, #71064, #46561, #91786, #34857, #32960, #68299, #11731, #53147, #27845, #90271, #19307, #22716, #97614, #56590, #46186, #43374, #11109, #71147, #84610, #32834, #10669, #48593, #9844, #36942, #27501, #96096, #37820, #90931, #17769, #54799, #44061, #91719, #96990, #3687, #61113, #54061, #84897, #89142, #48586, #64837, #89054, #62224, #54038, #93591, #22204, #72556, #72040, #72104, #34433, #47589, #60452, #90611, #67928, #3411, #1180, #22668, #30964, #94276, #62428, #95672, #254, #81324, #44818, #3134, #29861, #57333, #85986, #59389, #19009, #55918, #63273, #75274, #48986, #7747, #56354, #9884, #54422, #3812, #67285, #51792, #21739, #61381, #41043, #73403, #19940, #100076, #73895, #17296, #66566, #98463, #16870, #1938, #16197, #58168, #95498, #8787, #98829, #66116, #16586, #6262, #12225, #97794, #75599, #63609, #49856, #13501, #29728, #49975, #21478, #92376, #46080, #54630, #30399, #78728, #44191, #52879, #15503, #36553, #9409, #20229, #21626, #21220, #56975, #97020, #34946, #42037, #28860, #80031, #48746, #97347, #6357, #49164, #55577, #81489, #34456, #20878, #32724, #13131, #19623, #45192, #95385, #50200, #88051, #24746, #44816, #74292, #8241, #100081, #68529, #80002, #16589, #12398, #9766, #33184, #73176, #45071, #33254, #2172, #59171, #83712, #31482, #51686, #34259, #41580, #66055, #17355, #93853, #68891, #79622, #47067, #96390, #91298, #38358, #95245, #7119, #73784, #68914, #78460, #63969, #54943, #13392, #68468, #42682, #29982, #68798, #61412, #25368, #98251, #21091, #5262, #85499, #46304, #13253, #35585, #25718, #29864, #39032, #96504, #36572, #7082, #7468, #29189, #26724, #84506, #87491, #74520, #70127, #81599, #42268, #92537, #83467, #84128, #42209, #20206, #78363, #24896, #31431, #20615, #42620, #51418, #23566, #83294, #85822, #16973, #19901, #70947, #49343, #8196, #31576, #789, #10509, #34986, #60842, #95983, #25055, #56744, #75846, #66809, #72542, #48401, #27972, #37846, #36708, #55975, #2210, #80419, #28409, #88136, #75921, #53829, #97246, #71877, #6205, #70746, #75716, #14788, #30635, #79927, #23203, #2602, #82343, #82372, #18339, #33203, #35479, #46099, #29882, #20626, #74429, #21493, #59201, #89868, #39632, #34745, #64666, #28586, #1768, #19134, #7512, #59938, #79316, #72891, #15351, #73887, #9404, #73759, #86222, #62035, #88708, #60380, #88254, #94381, #68510, #95898, #47475, #14951, #56460, #35849, #27967, #96872, #58083, #93639, #95848, #51712, #1419, #87094, #57885, #83736, #66914, #16243, #19863, #94015, #13872, #12378, #68189, #3821, #7882, #71661, #18224, #58922, #81426, #43871, #17607, #46, #76284, #13997, #47198, #8574, #68032, #82048, #70164, #93717, #69770, #662, #81236, #25573, #78294, #70801, #20958, #87549, #46067, #5988, #98996, #40837, #97254, #20168, #47519, #45582, #20708, #92754, #91247, #64833, #51335, #28756, #22379, #74615, #67195, #66801, #42782, #11354, #67787, #1662, #100334, #61175, #38226, #95934, #22240, #25594, #47412, #82826, #44484, #38939, #50076, #40365, #20898, #461, #72836, #18142, #16952, #62041, #50725, #42318, #59520, #10909, #29972, #75197, #31887, #38176, #7383, #56722, #98968, #49328, #77240, #91113, #24054, #39967, #40761, #9030, #31878, #84323, #53565, #97816, #39245, #44098, #84423, #48949, #88538, #25353, #51700, #92735, #4900, #34807, #74264, #3279, #69112, #35396, #72312, #45485, #41718, #629, #39370, #28595, #1087, #49306, #71831, #58695, #9181, #14635, #52599, #38726, #43525, #16047, #28013, #40607, #60869, #625, #73814, #30979, #55107, #42488, #92632, #64846, #77976, #66915, #31833, #56775, #93584, #2070, #97146, #74631, #46590, #60299, #27026, #84388, #10391, #35418, #16485, #55972, #77409, #74027, #29734, #6523, #20484, #31355, #30842, #10190, #6494, #41735, #21866, #6397, #39055, #65561, #72775, #52533, #20707, #51457, #96345, #87521, #76117, #31177, #72883, #58339, #73026, #97646, #7268, #61924, #53615, #45314, #77750, #97940, #8140, #63572, #61202, #38827, #78236, #39070, #59806, #62955, #66088, #68553, #77649, #48274, #99371, #54970, #22921, #66934, #7650, #69392, #94738, #23953, #3672, #86247, #43473, #66280, #57404, #55275, #56693, #7246, #43086, #38442, #37044, #43943, #43067, #98567, #34587, #11085, #46720, #27046, #27758, #33996, #70906, #93707, #71792, #78106, #93576, #33262, #21880, #53706, #1760, #71022, #5723, #3155, #11078, #3251, #73740, #96052, #86863, #13129, #63443, #39546, #43764, #20750, #23910, #73200, #87133, #58642, #42342, #40100, #92258, #9978, #39075, #54211, #93504, #26951, #41844, #35609, #77829, #15343, #10516, #593, #86523, #44204, #15823, #26973, #67674, #20091, #53567, #82203, #54592, #4909, #92080, #375, #74038, #63199, #4468, #15622, #6157, #96518, #97570, #32743, #73165, #42711, #53087, #47489, #82133, #96316, #25076, #73553, #76988, #12996, #16726, #94307, #34317, #42508, #7508, #2054, #11420, #92646, #95250, #91466, #10408, #74280, #21701, #17383, #42389, #42893, #36983, #56628, #30187, #94719, #12027, #50068, #33223, #41086, #3921, #15755, #31341, #70490, #27584, #63327, #33134, #43722, #34990, #28921, #91620, #41339, #76488, #59449, #31449, #89042, #27411, #36073, #44463, #34873, #19834, #24345, #60550, #66615, #38597, #73382, #9668, #48735, #64717, #99187, #36104, #24165, #90254, #47570, #92637, #10632, #8011, #69531, #10388, #8863, #89909, #35267, #30596, #30446, #10151, #67686 ) ) ;
#72027=EDGE_LOOP ( 'NONE', ( #17628, #52766, #31986, #90856 ) ) ;
#72029=CARTESIAN_POINT ( 'NONE',  ( 20.35648204094723468, -10.72454223111430593, 11.49999999999998934 ) ) ;
#72031=VERTEX_POINT ( 'NONE', #1442 ) ;
#72033=CARTESIAN_POINT ( 'NONE',  ( -118.5895376238167245, -24.65952944569304961, 1.056160979905702346 ) ) ;
#72034=B_SPLINE_CURVE_WITH_KNOTS ( 'NONE', 3,
 ( #24975, #71166, #31085, #53946, #22954, #46321 ),
 .UNSPECIFIED., .F., .F.,
 ( 4, 2, 4 ),
 ( 0.000000000000000000, 0.001380764517854761279, 0.002761529035709522559 ),
 .UNSPECIFIED. ) ;
#72036=DIRECTION ( 'NONE',  ( -3.773278334453079618E-23, 0.9999999999976377785, 2.173523156925978705E-06 ) ) ;
#72038=CARTESIAN_POINT ( 'NONE',  ( -21.20786952941880443, -2.223526401999901925, 11.49999999999999645 ) ) ;
#72039=ORIENTED_EDGE ( 'NONE', *, *, #82022, .T. ) ;
#72040=ORIENTED_EDGE ( 'NONE', *, *, #3775, .F. ) ;
#72041=CARTESIAN_POINT ( 'NONE',  ( -22.15176777451872425, 1.842445310382735624, -1.500000000000002220 ) ) ;
#72042=CARTESIAN_POINT ( 'NONE',  ( 16.46467569749531634, 12.45148609503053017, 11.49999999999998934 ) ) ;
#72044=EDGE_CURVE ( 'NONE', #93818, #46475, #7541, .T. ) ;
#72045=ORIENTED_EDGE ( 'NONE', *, *, #99069, .T. ) ;
#72047=CARTESIAN_POINT ( 'NONE',  ( -71.72404080852884078, -25.30060019737137367, 6.009288023823078362 ) ) ;
#72048=ORIENTED_EDGE ( 'NONE', *, *, #67143, .F. ) ;
#72049=CARTESIAN_POINT ( 'NONE',  ( -95.52287095715004739, -23.47593901973090169, -1.443836447538996648 ) ) ;
#72050=ORIENTED_EDGE ( 'NONE', *, *, #63940, .T. ) ;
#72053=CARTESIAN_POINT ( 'NONE',  ( 11.47802407633690258, -17.41396394059345454, -1.500000000000002220 ) ) ;
#72054=CARTESIAN_POINT ( 'NONE',  ( -21.73523922981167189, -2.474665994198115726, 11.49999999999999645 ) ) ;
#72056=VECTOR ( 'NONE', #40956, 1000.000000000000114 ) ;
#72058=CARTESIAN_POINT ( 'NONE',  ( -122.5228709571500616, -29.50248528299804818, 1.056150453629045360 ) ) ;
#72059=CARTESIAN_POINT ( 'NONE',  ( -11.50411854321151672, 19.32100693743031528, 11.49999999999998934 ) ) ;
#72060=CARTESIAN_POINT ( 'NONE',  ( 8.587038044527741221, -19.06309208085484386, 11.49999999999998934 ) ) ;
#72061=ADVANCED_FACE ( 'NONE', ( #26768 ), #96281, .T. ) ;
#72062=CARTESIAN_POINT ( 'NONE',  ( -38.62372276496436996, -24.65952944569304606, 1.056160979905694131 ) ) ;
#72063=CARTESIAN_POINT ( 'NONE',  ( -72.52287095715010423, -24.66019654487199375, 8.947790411086128159 ) ) ;
#72065=EDGE_LOOP ( 'NONE', ( #52287, #3404, #83625, #59362 ) ) ;
#72066=EDGE_CURVE ( 'NONE', #69390, #22695, #34882, .T. ) ;
#72067=VERTEX_POINT ( 'NONE', #10041 ) ;
#72069=CARTESIAN_POINT ( 'NONE',  ( -52.50767261960347554, -23.96119346886881019, -0.6495511937831939253 ) ) ;
#72071=B_SPLINE_CURVE_WITH_KNOTS ( 'NONE', 3,
 ( #17482, #40819, #17986, #49453 ),
 .UNSPECIFIED., .F., .F.,
 ( 4, 4 ),
 ( 0.000000000000000000, 9.999999999998898659E-05 ),
 .UNSPECIFIED. ) ;
#72072=CARTESIAN_POINT ( 'NONE',  ( 13.27131465344908001, -16.79725507166503462, -1.500000000000002220 ) ) ;
#72073=CARTESIAN_POINT ( 'NONE',  ( 11.21425909587273928, 19.38466839394011387, 11.49999999999999645 ) ) ;
#72074=ORIENTED_EDGE ( 'NONE', *, *, #96045, .F. ) ;
#72076=CARTESIAN_POINT ( 'NONE',  ( 20.56459456670464547, 4.482388377596099538, -1.500000000000002220 ) ) ;
#72077=CARTESIAN_POINT ( 'NONE',  ( -30.45987998222503634, -25.30657267508212271, 5.002391647799127483 ) ) ;
#72078=CARTESIAN_POINT ( 'NONE',  ( 5.901097582950029619, 19.04237314665466485, -1.500000000000002220 ) ) ;
#72080=DIRECTION ( 'NONE',  ( -3.773278334453080206E-23, 0.9999999999976377785, 2.173523156925979975E-06 ) ) ;
#72081=CARTESIAN_POINT ( 'NONE',  ( -14.94409825380703616, 16.19114737329946507, -1.500000000000002220 ) ) ;
#72083=CARTESIAN_POINT ( 'NONE',  ( -65.48565164118330983, -24.92592662359560762, 8.075495903017996469 ) ) ;
#72084=CARTESIAN_POINT ( 'NONE',  ( -111.6228709571500701, -23.48786465467241769, 11.44779295918254114 ) ) ;
#72085=CARTESIAN_POINT ( 'NONE',  ( -63.58953762381672448, -23.47593901973091235, -1.443836447539007972 ) ) ;
#72086=CARTESIAN_POINT ( 'NONE',  ( -47.52287095715008292, -24.33832256527048088, 0.1851278514138576248 ) ) ;
#72090=CARTESIAN_POINT ( 'NONE',  ( 3.515848477382193416, 21.04717058667041130, -1.500000000000002220 ) ) ;
#72091=CARTESIAN_POINT ( 'NONE',  ( -40.52287095715006870, -29.50250243563736774, 8.947779886222148704 ) ) ;
#72092=LINE ( 'NONE', #8678, #62715 ) ;
#72094=DIRECTION ( 'NONE',  ( -0.000000000000000000, 2.173523156925979552E-06, -0.9999999999976378895 ) ) ;
#72095=CARTESIAN_POINT ( 'NONE',  ( -19.94007547503736788, -10.58355046294204094, -1.500000000000002220 ) ) ;
#72099=CARTESIAN_POINT ( 'NONE',  ( -120.5228709571500616, -23.47596703998600631, 11.44779298504227860 ) ) ;
#72100=CARTESIAN_POINT ( 'NONE',  ( -17.62575346185542102, 8.740161020289619387, 11.49999999999999645 ) ) ;
#72103=B_SPLINE_CURVE_WITH_KNOTS ( 'NONE', 3,
 ( #88598, #10461, #41421, #64788 ),
 .UNSPECIFIED., .F., .F.,
 ( 4, 4 ),
 ( 0.000000000000000000, 9.999999999998206125E-05 ),
 .UNSPECIFIED. ) ;
#72104=ORIENTED_EDGE ( 'NONE', *, *, #95524, .F. ) ;
#72105=DIRECTION ( 'NONE',  ( 3.773278334444165844E-23, -1.000000000000000000, 0.000000000000000000 ) ) ;
#72106=CARTESIAN_POINT ( 'NONE',  ( -127.4728709571500360, -25.40675522342679926, 5.000950437786769953 ) ) ;
#72108=CARTESIAN_POINT ( 'NONE',  ( -88.58953762381671027, -23.47593901973091235, -1.443836447539002865 ) ) ;
#72111=CARTESIAN_POINT ( 'NONE',  ( -19.76903914530799966, 0.2396048511829373395, 11.49999999999998934 ) ) ;
#72113=CARTESIAN_POINT ( 'NONE',  ( 3.706880958665978998, 19.89330832657401515, 11.49999999999999645 ) ) ;
#72116=ORIENTED_EDGE ( 'NONE', *, *, #32875, .T. ) ;
#72118=CARTESIAN_POINT ( 'NONE',  ( -69.34303308397305443, -25.24554880456021522, 6.209207408033732278 ) ) ;
#72119=CARTESIAN_POINT ( 'NONE',  ( -50.51883597636249590, -25.30394825761364785, 5.202350221066103231 ) ) ;
#72120=CARTESIAN_POINT ( 'NONE',  ( -82.62287095715005592, -24.64898659630367916, 1.056161002820826145 ) ) ;
#72123=EDGE_CURVE ( 'NONE', #80787, #34855, #21173, .T. ) ;
#72124=CARTESIAN_POINT ( 'NONE',  ( -120.5228709571500616, -23.48786465467241769, 11.44779295918253759 ) ) ;
#72125=CARTESIAN_POINT ( 'NONE',  ( -19.63739455291241498, 3.909132673056371132, 11.49999999999998934 ) ) ;
#72127=EDGE_CURVE ( 'NONE', #15143, #90740, #33882, .T. ) ;
#72128=CARTESIAN_POINT ( 'NONE',  ( -117.6228709571500559, -24.64898659630368627, 1.056161002820833028 ) ) ;
#72129=ORIENTED_EDGE ( 'NONE', *, *, #25599, .F. ) ;
#72130=ADVANCED_FACE ( 'NONE', ( #42011 ), #65858, .T. ) ;
#72131=EDGE_CURVE ( 'NONE', #50353, #27980, #57508, .T. ) ;
#72132=CARTESIAN_POINT ( 'NONE',  ( -73.62287095715007013, -24.33927499327854704, 9.819080762295822495 ) ) ;
#72133=CARTESIAN_POINT ( 'NONE',  ( -35.64144378499706534, -24.52300882791529446, 0.6510814631126419227 ) ) ;
#72134=LINE ( 'NONE', #71625, #37046 ) ;
#72135=CARTESIAN_POINT ( 'NONE',  ( -119.4728709571500644, -25.40558663563398056, 5.000950440326719537 ) ) ;
#72136=CARTESIAN_POINT ( 'NONE',  ( -101.6837879195638124, -25.23386281078603943, 3.681742193200927105 ) ) ;
#72138=CARTESIAN_POINT ( 'NONE',  ( -98.87408511115022236, -25.31392319263090585, 5.203681702801228326 ) ) ;
#72140=CARTESIAN_POINT ( 'NONE',  ( 19.34776771173714849, 6.126202725962671458, 11.49999999999998934 ) ) ;
#72141=ORIENTED_EDGE ( 'NONE', *, *, #77818, .T. ) ;
#72142=EDGE_CURVE ( 'NONE', #92874, #96665, #56251, .T. ) ;
#72144=CARTESIAN_POINT ( 'NONE',  ( -96.52287095715007581, -23.47593901973090524, -1.443836447538996648 ) ) ;
#72145=CARTESIAN_POINT ( 'NONE',  ( -59.50358786707867154, -24.15620529776628089, 10.23563542870661180 ) ) ;
#72146=CARTESIAN_POINT ( 'NONE',  ( -86.52287095715009002, -23.96177878511310055, 10.65340807706330217 ) ) ;
#72148=CARTESIAN_POINT ( 'NONE',  ( -30.47287095715006444, -25.29799310117780919, 4.442956538296639835 ) ) ;
#72149=CARTESIAN_POINT ( 'NONE',  ( 6.139388171429570384, 20.22809724653347985, 11.49999999999999645 ) ) ;
#72151=CARTESIAN_POINT ( 'NONE',  ( 10.50125231818214289, 19.49540335892314502, 11.49999999999998934 ) ) ;
#72152=CARTESIAN_POINT ( 'NONE',  ( -19.32567751138619982, -7.045664331180771178, -1.500000000000002220 ) ) ;
#72155=VERTEX_POINT ( 'NONE', #49126 ) ;
#72156=CARTESIAN_POINT ( 'NONE',  ( -54.63281596392198480, -24.34968618360932879, 0.1864209137778771175 ) ) ;
#72157=CARTESIAN_POINT ( 'NONE',  ( -80.52287095715006160, -23.47593901973090169, -1.443836447538996648 ) ) ;
#72160=B_SPLINE_CURVE_WITH_KNOTS ( 'NONE', 3,
 ( #32000, #39611, #70562, #55354 ),
 .UNSPECIFIED., .F., .F.,
 ( 4, 4 ),
 ( 0.000000000000000000, 1.000000000000000000 ),
 .UNSPECIFIED. ) ;
#72162=CARTESIAN_POINT ( 'NONE',  ( -111.7078649355182023, -25.26111664902047238, 3.848907687874172812 ) ) ;
#72163=PLANE ( 'NONE',  #97271 ) ;
#72165=CARTESIAN_POINT ( 'NONE',  ( -4.968023186724614959, -20.10795263665959709, -1.500000000000002220 ) ) ;
#72166=CARTESIAN_POINT ( 'NONE',  ( -11.49108604648090548, 18.38894055434275643, 11.49999999999999645 ) ) ;
#72168=CARTESIAN_POINT ( 'NONE',  ( -60.52287095715007581, -25.00182538069855198, 7.747789668514453609 ) ) ;
#72170=CARTESIAN_POINT ( 'NONE',  ( 21.16571772479873204, -7.350578744355993344, -1.500000000000002220 ) ) ;
#72173=CARTESIAN_POINT ( 'NONE',  ( -27.68651082257922980, -24.78174777341091328, 2.274903344755643708 ) ) ;
#72174=EDGE_LOOP ( 'NONE', ( #17862, #41999, #22198, #83034 ) ) ;
#72176=CARTESIAN_POINT ( 'NONE',  ( -35.67969092473991566, -23.48786465467240703, 11.44779295918255180 ) ) ;
#72179=ADVANCED_FACE ( 'NONE', ( #60227 ), #62110, .T. ) ;
#72181=CARTESIAN_POINT ( 'NONE',  ( -70.62287095715007013, -23.47596703998600631, 11.44779298504227505 ) ) ;
#72182=ORIENTED_EDGE ( 'NONE', *, *, #12213, .F. ) ;
#72183=PLANE ( 'NONE',  #73015 ) ;
#72184=CARTESIAN_POINT ( 'NONE',  ( -20.82729772986975547, -4.079710536234080642, -1.500000000000002220 ) ) ;
#72186=CARTESIAN_POINT ( 'NONE',  ( -88.54318482745297558, -24.65952944569304606, 1.056160979905701902 ) ) ;
#72187=CARTESIAN_POINT ( 'NONE',  ( -11.22809577558575000, 18.72649003030000259, -1.500000000000002220 ) ) ;
#72188=CARTESIAN_POINT ( 'NONE',  ( -103.5530466354624508, -24.15620529776628445, 10.23563542870660292 ) ) ;
#72190=DIRECTION ( 'NONE',  ( 3.773278334444166432E-23, -1.000000000000000000, 0.000000000000000000 ) ) ;
#72191=CARTESIAN_POINT ( 'NONE',  ( 19.28182042344761626, 10.37885539243483812, -1.500000000000002220 ) ) ;
#72197=ORIENTED_EDGE ( 'NONE', *, *, #42916, .T. ) ;
#72199=VERTEX_POINT ( 'NONE', #37379 ) ;
#72203=CARTESIAN_POINT ( 'NONE',  ( 21.11169859150035677, 2.410084449224629832, 11.49999999999998934 ) ) ;
#72205=CARTESIAN_POINT ( 'NONE',  ( -40.43801387148943149, -25.26938797564855932, 6.123095479407366426 ) ) ;
#72206=PLANE ( 'NONE',  #77783 ) ;
#72207=CARTESIAN_POINT ( 'NONE',  ( -112.6228709571500559, -29.50248528299804818, 1.056150453629043584 ) ) ;
#72208=CARTESIAN_POINT ( 'NONE',  ( -13.34961138979462270, 14.11212085816309880, 11.49999999999998934 ) ) ;
#72209=CARTESIAN_POINT ( 'NONE',  ( -80.62287095715004170, -23.48786465467241058, 11.44779295918254469 ) ) ;
#72210=EDGE_LOOP ( 'NONE', ( #46315, #19584, #31935, #75000 ) ) ;
#72211=CARTESIAN_POINT ( 'NONE',  ( 16.96702763494397104, -9.608290155750392358, 11.49999999999999645 ) ) ;
#72214=VERTEX_POINT ( 'NONE', #90656 ) ;
#72215=CARTESIAN_POINT ( 'NONE',  ( -58.62287095715004881, -23.72773821059535848, 11.05748984161097503 ) ) ;
#72216=CARTESIAN_POINT ( 'NONE',  ( -89.59466492980996577, -23.96119346886881019, -0.6495511937831908167 ) ) ;
#72217=B_SPLINE_CURVE_WITH_KNOTS ( 'NONE', 3,
 ( #53300, #77111, #92345, #29951, #44689, #98956, #22818, #38061 ),
 .UNSPECIFIED., .F., .F.,
 ( 4, 2, 2, 4 ),
 ( 0.000000000000000000, 0.002001098010032686253, 0.003001647015049031114, 0.004002196020065375975 ),
 .UNSPECIFIED. ) ;
#72219=CARTESIAN_POINT ( 'NONE',  ( -81.13115756185166560, -25.03156031351837996, 7.427330859781487327 ) ) ;
#72220=CARTESIAN_POINT ( 'NONE',  ( -14.15603575923578283, -13.64839490926926580, -1.500000000000002220 ) ) ;
#72221=ORIENTED_EDGE ( 'NONE', *, *, #94187, .F. ) ;
#72223=CARTESIAN_POINT ( 'NONE',  ( -78.52287095715009002, -23.96127896941631974, -0.6493128931038031348 ) ) ;
#72224=CARTESIAN_POINT ( 'NONE',  ( -14.75821945985506645, 17.75411527500383002, -1.500000000000002220 ) ) ;
#72225=SHAPE_DEFINITION_REPRESENTATION ( #96842, #37291 ) ;
#72227=CARTESIAN_POINT ( 'NONE',  ( -83.62287095715005592, -29.50250243563736774, 8.947779886222141599 ) ) ;
#72228=CARTESIAN_POINT ( 'NONE',  ( -108.9545715455115129, -25.27705962214097113, 4.170144839539424275 ) ) ;
#72229=CARTESIAN_POINT ( 'NONE',  ( -97.51608334452220106, -23.96169478059713853, 10.65365249895717703 ) ) ;
#72230=CARTESIAN_POINT ( 'NONE',  ( -114.6228709571500417, -24.65952944569305316, 1.056160979905703234 ) ) ;
#72233=CARTESIAN_POINT ( 'NONE',  ( -69.34512923434627396, -25.24515217105749443, 6.118189401617559753 ) ) ;
#72234=CARTESIAN_POINT ( 'NONE',  ( -50.62287095715005592, -23.47593901973091235, -1.443836447539009749 ) ) ;
#72235=CARTESIAN_POINT ( 'NONE',  ( -19.80664267627650688, 2.137978742899185214, 11.49999999999998934 ) ) ;
#72237=CARTESIAN_POINT ( 'NONE',  ( -75.58684609491236017, -24.63419186844611275, 9.035850630976923981 ) ) ;
#72238=CARTESIAN_POINT ( 'NONE',  ( -19.84341114293531305, -1.032944114202840824, -1.500000000000002220 ) ) ;
#72239=ORIENTED_EDGE ( 'NONE', *, *, #30630, .F. ) ;
#72240=PLANE ( 'NONE',  #28118 ) ;
#72243=EDGE_CURVE ( 'NONE', #937, #81281, #87681, .T. ) ;
#72244=PLANE ( 'NONE',  #84091 ) ;
#72245=CARTESIAN_POINT ( 'NONE',  ( -93.52287095715006160, -24.66019654487200086, 8.947790411086110396 ) ) ;
#72247=CARTESIAN_POINT ( 'NONE',  ( 15.20108283357335921, -14.20388156210760577, 11.49999999999999645 ) ) ;
#72248=CARTESIAN_POINT ( 'NONE',  ( -37.92287095715006018, -23.47593901973090169, -1.443836447538997980 ) ) ;
#72251=CARTESIAN_POINT ( 'NONE',  ( -16.39533425382319720, 15.89506036719111037, 11.49999999999999645 ) ) ;
#72254=LINE ( 'NONE', #49425, #51139 ) ;
#72255=DIRECTION ( 'NONE',  ( 3.773278334444166432E-23, -1.000000000000000000, 0.000000000000000000 ) ) ;
#72256=ORIENTED_EDGE ( 'NONE', *, *, #33054, .T. ) ;
#72258=CARTESIAN_POINT ( 'NONE',  ( -5.148175472751820081, -19.54457232503198227, -1.500000000000002220 ) ) ;
#72260=AXIS2_PLACEMENT_3D ( 'NONE', #100116, #69200, #28771 ) ;
#72261=CARTESIAN_POINT ( 'NONE',  ( -114.5562042904833930, -24.66019654487199730, 8.947790411086124607 ) ) ;
#72263=EDGE_CURVE ( 'NONE', #59988, #20176, #23484, .T. ) ;
#72264=CARTESIAN_POINT ( 'NONE',  ( -100.6228709571500701, -24.63287334234177450, 0.9662140553045522884 ) ) ;
#72266=CARTESIAN_POINT ( 'NONE',  ( -70.62287095715004170, -24.91570333823099759, 8.075032458375549282 ) ) ;
#72268=CARTESIAN_POINT ( 'NONE',  ( -10.14125802585430947, 17.27231531754821603, -1.500000000000002220 ) ) ;
#72269=CARTESIAN_POINT ( 'NONE',  ( 19.40473180639871131, -7.901900427366274293, 11.49999999999999645 ) ) ;
#72270=CARTESIAN_POINT ( 'NONE',  ( -27.79917671128472634, -24.65826116135614754, 8.250243081618606311 ) ) ;
#72271=CARTESIAN_POINT ( 'NONE',  ( -70.48669436695099932, -25.00182538069146787, 7.747789668545044250 ) ) ;
#72272=CARTESIAN_POINT ( 'NONE',  ( 19.60348439636399931, 10.09110264789753053, -1.500000000000002220 ) ) ;
#72273=CARTESIAN_POINT ( 'NONE',  ( -42.55620429048339304, -24.64898659630528144, 1.056161002820814154 ) ) ;
#72274=ORIENTED_EDGE ( 'NONE', *, *, #18285, .T. ) ;
#72276=CARTESIAN_POINT ( 'NONE',  ( -118.5228709571501184, -24.35013146730205236, 9.818937971375092388 ) ) ;
#72277=CARTESIAN_POINT ( 'NONE',  ( -50.58953762381673158, -24.99132157543083821, 2.256160258750496084 ) ) ;
#72278=ORIENTED_EDGE ( 'NONE', *, *, #77232, .F. ) ;
#72279=PLANE ( 'NONE',  #58338 ) ;
#72280=ORIENTED_EDGE ( 'NONE', *, *, #75313, .T. ) ;
#72284=CARTESIAN_POINT ( 'NONE',  ( -58.62287095715004170, -23.73907113216990794, -1.053371485793233919 ) ) ;
#72285=CARTESIAN_POINT ( 'NONE',  ( 20.20254288951482735, -3.758238384022974277, -1.500000000000002220 ) ) ;
#72290=CARTESIAN_POINT ( 'NONE',  ( 16.98343680692684643, -14.46476453587665389, 11.49999999999998934 ) ) ;
#72291=CARTESIAN_POINT ( 'NONE',  ( -55.52287095715006870, -23.48786465467241058, 11.44779295918254824 ) ) ;
#72292=ORIENTED_EDGE ( 'NONE', *, *, #84028, .F. ) ;
#72294=CARTESIAN_POINT ( 'NONE',  ( -65.55620429048339304, -24.99132157543166599, 2.256160258750668390 ) ) ;
#72295=CARTESIAN_POINT ( 'NONE',  ( -11.21968731015968856, -17.59241007644406096, -1.500000000000002220 ) ) ;
#72298=ORIENTED_EDGE ( 'NONE', *, *, #53757, .F. ) ;
#72299=VERTEX_POINT ( 'NONE', #12532 ) ;
#72300=CARTESIAN_POINT ( 'NONE',  ( -70.15801421577009478, -25.03149371388890643, 7.556454810261096000 ) ) ;
#72301=CARTESIAN_POINT ( 'NONE',  ( 20.15827220212406701, 6.050813824765241655, -1.500000000000002220 ) ) ;
#72303=ORIENTED_EDGE ( 'NONE', *, *, #84407, .T. ) ;
#72306=CARTESIAN_POINT ( 'NONE',  ( -120.5177523882421582, -24.63419186844610920, 9.035850630976920428 ) ) ;
#72307=CARTESIAN_POINT ( 'NONE',  ( -86.51402387307511788, -23.96169478059713498, 10.65365249895717881 ) ) ;
#72308=CARTESIAN_POINT ( 'NONE',  ( -59.60445504388953708, -23.73766607897669445, -1.055555164236460675 ) ) ;
#72309=CARTESIAN_POINT ( 'NONE',  ( 19.26462925850498920, -9.998780574493274287, -1.500000000000002220 ) ) ;
#72311=CARTESIAN_POINT ( 'NONE',  ( -9.338385371603758145, -20.21602636099808237, 11.49999999999999645 ) ) ;
#72312=ORIENTED_EDGE ( 'NONE', *, *, #87565, .T. ) ;
#72313=CARTESIAN_POINT ( 'NONE',  ( -51.52443300084429723, -25.31441916312803286, 6.090564871685868020 ) ) ;
#72314=CARTESIAN_POINT ( 'NONE',  ( -30.64427850938830389, -23.56000036390796737, -1.497999999999532594 ) ) ;
#72315=EDGE_CURVE ( 'NONE', #76871, #1915, #6425, .T. ) ;
#72316=CARTESIAN_POINT ( 'NONE',  ( -70.48052921158478057, -25.30151219336677570, 5.317344105861852910 ) ) ;
#72317=ORIENTED_EDGE ( 'NONE', *, *, #10508, .F. ) ;
#72319=CARTESIAN_POINT ( 'NONE',  ( -65.62287095715005592, -29.50248789122583659, 2.256150453626215580 ) ) ;
#72322=LINE ( 'NONE', #2817, #80544 ) ;
#72325=CARTESIAN_POINT ( 'NONE',  ( -48.62287095715004881, -23.73907113216990794, -1.053371485793232143 ) ) ;
#72326=CARTESIAN_POINT ( 'NONE',  ( -66.52287095715006160, -24.33927499327855770, 9.819080762295810061 ) ) ;
#72328=VECTOR ( 'NONE', #32713, 1000.000000000000114 ) ;
#72329=CARTESIAN_POINT ( 'NONE',  ( -130.5728709571500588, -24.45096232750585585, 9.783294602970084242 ) ) ;
#72330=CARTESIAN_POINT ( 'NONE',  ( 12.67250375155129127, 18.46511205475877304, -1.500000000000002220 ) ) ;
#72333=ORIENTED_EDGE ( 'NONE', *, *, #1438, .T. ) ;
#72335=CARTESIAN_POINT ( 'NONE',  ( -112.5222218478034790, -23.48786465467241769, 11.44779295918253936 ) ) ;
#72336=CARTESIAN_POINT ( 'NONE',  ( -55.62287095715004170, -23.47596703998600631, 11.44779298504227505 ) ) ;
#72337=DIRECTION ( 'NONE',  ( -1.000000000000000000, -3.773278334444166432E-23, -8.201307841325785021E-29 ) ) ;
#72338=CARTESIAN_POINT ( 'NONE',  ( -48.62287095715004881, -23.47593901973091235, -1.443836447539009749 ) ) ;
#72340=B_SPLINE_CURVE_WITH_KNOTS ( 'NONE', 3,
 ( #49294, #87327, #34554, #41678 ),
 .UNSPECIFIED., .F., .F.,
 ( 4, 4 ),
 ( 1.387778780781445521E-17, 9.999999999997510880E-05 ),
 .UNSPECIFIED. ) ;
#72341=CARTESIAN_POINT ( 'NONE',  ( -97.23961514226040492, -25.30557784678704536, 3.856996771331004048 ) ) ;
#72342=CARTESIAN_POINT ( 'NONE',  ( 3.528372621398383924, 19.26332229581237598, -1.500000000000002220 ) ) ;
#72343=CARTESIAN_POINT ( 'NONE',  ( -59.58953762381671027, -24.65952944569304250, 1.056160979905690134 ) ) ;
#72345=CARTESIAN_POINT ( 'NONE',  ( -0.8555947871142663974, 21.52075748220454798, 11.49999999999998934 ) ) ;
#72348=CARTESIAN_POINT ( 'NONE',  ( -100.8359211054894899, -25.12990627727104354, 2.884779682363133535 ) ) ;
#72349=CARTESIAN_POINT ( 'NONE',  ( 6.026614999332422182E-17, -23.47594215783195537, -5.102550391006585557E-05 ) ) ;
#72350=CARTESIAN_POINT ( 'NONE',  ( 1.269710630819723463, 22.90746787927615102, -1.500000000000002220 ) ) ;
#72353=CARTESIAN_POINT ( 'NONE',  ( -49.56034765714075263, -23.73766607897670156, -1.055555164236457566 ) ) ;
#72354=CARTESIAN_POINT ( 'NONE',  ( -20.11654390397962544, -0.4351469013266864860, 11.49999999999999645 ) ) ;
#72359=B_SPLINE_CURVE_WITH_KNOTS ( 'NONE', 3,
 ( #40062, #17214, #42074, #11103, #32950, #41570, #78595, #95342, #18705, #95841, #73019, #49685, #56804, #56305, #25829, #94837, #3010, #79613, #87225, #9606 ),
 .UNSPECIFIED., .F., .F.,
 ( 4, 2, 2, 2, 2, 2, 2, 2, 2, 4 ),
 ( 0.000000000000000000, 0.0004282660737508323275, 0.0008565321475016646549, 0.001284798221252496982, 0.001713064295003329310, 0.002141330368754161637, 0.002569596442504993965, 0.002997862516255826292, 0.003211995553131242673, 0.003426128590006658620 ),
 .UNSPECIFIED. ) ;
#72361=CARTESIAN_POINT ( 'NONE',  ( -77.52287095715006160, -29.50250786944525672, 11.44777988621623521 ) ) ;
#72362=CARTESIAN_POINT ( 'NONE',  ( 19.22361159462649027, -4.937694622890139939, -1.500000000000002220 ) ) ;
#72363=CARTESIAN_POINT ( 'NONE',  ( -90.62287095715008434, -23.85229601348995843, 10.88205029486209696 ) ) ;
#72364=CARTESIAN_POINT ( 'NONE',  ( -18.76583335001664565, 6.068782795689376286, -1.500000000000002220 ) ) ;
#72370=CARTESIAN_POINT ( 'NONE',  ( -60.52287095715007581, -23.84081130425356321, 10.88220057483158243 ) ) ;
#72371=CARTESIAN_POINT ( 'NONE',  ( -39.56136241089613037, -25.29384247623274362, 5.536731341526268224 ) ) ;
#72372=CARTESIAN_POINT ( 'NONE',  ( 19.88596897151998633, -5.565664080715476913, 11.49999999999999645 ) ) ;
#72374=EDGE_CURVE ( 'NONE', #69390, #51679, #45261, .T. ) ;
#72376=CARTESIAN_POINT ( 'NONE',  ( -13.31036990564671818, -18.29084955798148471, 11.49999999999999645 ) ) ;
#72377=ORIENTED_EDGE ( 'NONE', *, *, #64036, .T. ) ;
#72378=CARTESIAN_POINT ( 'NONE',  ( -69.34303308397305443, -25.12218950775438842, 6.209207676158020384 ) ) ;
#72379=CARTESIAN_POINT ( 'NONE',  ( -109.6228709571500559, -24.64965695001469115, 8.947790433994176951 ) ) ;
#72380=CARTESIAN_POINT ( 'NONE',  ( -39.62287095715004170, -24.33832256526968507, 0.1851278514119840124 ) ) ;
#72381=B_SPLINE_CURVE_WITH_KNOTS ( 'NONE', 3,
 ( #88736, #27823, #64921, #41565 ),
 .UNSPECIFIED., .F., .F.,
 ( 4, 4 ),
 ( 0.000000000000000000, 9.999999999999592548E-05 ),
 .UNSPECIFIED. ) ;
#72383=CARTESIAN_POINT ( 'NONE',  ( -27.70544111104076990, -24.93063634934924266, 8.251826098080067950 ) ) ;
#72386=ORIENTED_EDGE ( 'NONE', *, *, #16200, .T. ) ;
#72387=FACE_OUTER_BOUND ( 'NONE', #86409, .T. ) ;
#72388=CARTESIAN_POINT ( 'NONE',  ( -12.33899560737860313, 19.21699747222852395, -1.500000000000002220 ) ) ;
#72389=CARTESIAN_POINT ( 'NONE',  ( -98.55620429048337883, -24.64965694238575011, 8.947790433994191162 ) ) ;
#72390=CARTESIAN_POINT ( 'NONE',  ( -96.55486200352346771, -23.96119346886881019, -0.6495511937832061378 ) ) ;
#72391=CARTESIAN_POINT ( 'NONE',  ( -63.52208778886303264, -23.48786465467241058, 11.44779295918254824 ) ) ;
#72392=CARTESIAN_POINT ( 'NONE',  ( 22.48569338394020534, -0.9006126209707296937, 11.49999999999999645 ) ) ;
#72393=ORIENTED_EDGE ( 'NONE', *, *, #158, .T. ) ;
#72394=CARTESIAN_POINT ( 'NONE',  ( -43.57658755379780757, -24.65952944569304606, 1.056160979905693909 ) ) ;
#72395=CARTESIAN_POINT ( 'NONE',  ( 21.10488023177059347, -6.046698511884514460, 11.49999999999998934 ) ) ;
#72396=CARTESIAN_POINT ( 'NONE',  ( -126.7287160163637054, -25.33540118152307485, 3.690489000554315169 ) ) ;
#72398=CARTESIAN_POINT ( 'NONE',  ( -111.5920145005471653, -23.96119346886881019, -0.6495511937832035843 ) ) ;
#72399=CARTESIAN_POINT ( 'NONE',  ( -118.5895376238167529, -23.48783264082478794, -1.443836473390058384 ) ) ;
#72400=ORIENTED_EDGE ( 'NONE', *, *, #74081, .T. ) ;
#72401=CARTESIAN_POINT ( 'NONE',  ( -48.57733566618777132, -24.66019654487199730, 8.947790411086119278 ) ) ;
#72404=AXIS2_PLACEMENT_3D ( 'NONE', #17371, #141, #71668 ) ;
#72405=CARTESIAN_POINT ( 'NONE',  ( -68.62287095715005592, -23.47596703998600631, 11.44779298504227505 ) ) ;
#72406=CARTESIAN_POINT ( 'NONE',  ( 19.38413035786728145, -6.671778716439519030, -1.500000000000002220 ) ) ;
#72409=ORIENTED_EDGE ( 'NONE', *, *, #44028, .F. ) ;
#72410=VERTEX_POINT ( 'NONE', #93640 ) ;
#72411=CARTESIAN_POINT ( 'NONE',  ( -67.52287095715006160, -23.47596703998600631, 11.44779298504228748 ) ) ;
#72412=CARTESIAN_POINT ( 'NONE',  ( 5.194767643164344584, 22.50260600399833422, -1.500000000000002220 ) ) ;
#72413=CARTESIAN_POINT ( 'NONE',  ( -104.5889232684893670, -24.35071581493543746, 9.817618358456019934 ) ) ;
#72414=CARTESIAN_POINT ( 'NONE',  ( 16.70477854660759931, 11.60849435585976153, -1.500000000000002220 ) ) ;
#72419=ADVANCED_FACE ( 'NONE', ( #305 ), #78917, .F. ) ;
#72420=CARTESIAN_POINT ( 'NONE',  ( -93.62287095715005592, -23.72773821059536559, 11.05748984161097681 ) ) ;
#72422=VERTEX_POINT ( 'NONE', #85032 ) ;
#72423=CARTESIAN_POINT ( 'NONE',  ( -28.66129012810275256, -25.21531751186669013, 2.702368919224620747 ) ) ;
#72424=CARTESIAN_POINT ( 'NONE',  ( -93.52287095715009002, -23.72773821059536914, 11.05748984161097326 ) ) ;
#72425=ORIENTED_EDGE ( 'NONE', *, *, #32972, .F. ) ;
#72426=CARTESIAN_POINT ( 'NONE',  ( -11.59579830748209517, 17.24510332420730663, -1.500000000000002220 ) ) ;
#72427=EDGE_LOOP ( 'NONE', ( #98759, #14387, #84637, #23099 ) ) ;
#72428=ADVANCED_FACE ( 'NONE', ( #76910 ), #38863, .T. ) ;
#72429=CARTESIAN_POINT ( 'NONE',  ( -125.6244081583916881, -24.52300882791529801, 0.6510814631126508045 ) ) ;
#72431=CARTESIAN_POINT ( 'NONE',  ( -41.52202759913466679, -23.48786465467240347, 11.44779295918255002 ) ) ;
#72435=FACE_OUTER_BOUND ( 'NONE', #85847, .T. ) ;
#72437=FACE_OUTER_BOUND ( 'NONE', #94313, .T. ) ;
#72438=CARTESIAN_POINT ( 'NONE',  ( 21.00647827173414939, 6.864759178008983831, 11.49999999999999645 ) ) ;
#72439=ORIENTED_EDGE ( 'NONE', *, *, #72807, .F. ) ;
#72440=CARTESIAN_POINT ( 'NONE',  ( -101.5562042904833930, -23.47596703998600631, 11.44779298504227683 ) ) ;
#72441=CARTESIAN_POINT ( 'NONE',  ( -17.80605238980536953, 13.89162706601689479, 11.49999999999998934 ) ) ;
#72442=LINE ( 'NONE', #2937, #21430 ) ;
#72444=ORIENTED_EDGE ( 'NONE', *, *, #26865, .T. ) ;
#72447=CARTESIAN_POINT ( 'NONE',  ( -57.57869602717082813, -24.66019654487199375, 8.947790411086119278 ) ) ;
#72449=CARTESIAN_POINT ( 'NONE',  ( 4.708956132399880978, 20.65895737721473679, 11.49999999999998934 ) ) ;
#72450=CARTESIAN_POINT ( 'NONE',  ( -44.52287095715006160, -24.64965694238575011, 8.947790433994205372 ) ) ;
#72451=CARTESIAN_POINT ( 'NONE',  ( -52.62287095715005592, -23.48786465467240703, 11.44779295918255002 ) ) ;
#72453=CARTESIAN_POINT ( 'NONE',  ( -80.62287095715008434, -24.92604778743018201, 8.074972756849359001 ) ) ;
#72454=CARTESIAN_POINT ( 'NONE',  ( 13.39142644571787422, -17.71860720625715757, -1.500000000000002220 ) ) ;
#72455=CARTESIAN_POINT ( 'NONE',  ( -114.6266393428067545, -24.15543982623908192, -0.2315651400026444429 ) ) ;
#72456=ORIENTED_EDGE ( 'NONE', *, *, #71347, .F. ) ;
#72459=CARTESIAN_POINT ( 'NONE',  ( 8.665315094346039970, 17.34094453737590769, 11.49999999999999645 ) ) ;
#72460=EDGE_CURVE ( 'NONE', #22234, #72609, #16249, .T. ) ;
#72461=VECTOR ( 'NONE', #54116, 1000.000000000000227 ) ;
#72462=CARTESIAN_POINT ( 'NONE',  ( -36.58681848114003543, -24.35071581493542325, 9.817618358456030592 ) ) ;
#72464=CARTESIAN_POINT ( 'NONE',  ( -19.44331071757236273, 1.017868325215548708, 11.49999999999998934 ) ) ;
#72465=CARTESIAN_POINT ( 'NONE',  ( 15.25824911148008844, 15.06768998368162471, -1.500000000000002220 ) ) ;
#72468=CARTESIAN_POINT ( 'NONE',  ( -51.53190491943575324, -24.65952944569304250, 1.056160979905695463 ) ) ;
#72469=CARTESIAN_POINT ( 'NONE',  ( -58.22287095715004313, -23.47593901973090169, -1.443836447538997758 ) ) ;
#72470=CARTESIAN_POINT ( 'NONE',  ( -20.26579564662877075, -10.28286414166031726, -1.500000000000002220 ) ) ;
#72474=CARTESIAN_POINT ( 'NONE',  ( -102.5474529007568378, -24.65952944569305316, 1.056160979905704123 ) ) ;
#72476=CARTESIAN_POINT ( 'NONE',  ( 13.74685606122050885, 14.44317598224977672, 11.49999999999999645 ) ) ;
#72477=CARTESIAN_POINT ( 'NONE',  ( -61.62287095715004881, -29.50248528299804818, 1.056150453629034924 ) ) ;
#72480=CARTESIAN_POINT ( 'NONE',  ( -48.62369540941691781, -24.65952944569304606, 1.056160979905697239 ) ) ;
#72483=PLANE ( 'NONE',  #34776 ) ;
#72484=CARTESIAN_POINT ( 'NONE',  ( -77.52287095715006160, -24.65952944569304606, 1.056160979905698794 ) ) ;
#72485=CARTESIAN_POINT ( 'NONE',  ( -18.79206335510377102, -10.79472360063173397, 11.49999999999998934 ) ) ;
#72486=CARTESIAN_POINT ( 'NONE',  ( -51.54694215012084157, -25.12787939889654609, 7.132508062825905881 ) ) ;
#72487=CARTESIAN_POINT ( 'NONE',  ( 19.40022266231057202, 1.907866353064612053, -1.500000000000002220 ) ) ;
#72488=DIRECTION ( 'NONE',  ( -1.000000000000000000, -3.773278334444166432E-23, -8.201307841325785021E-29 ) ) ;
#72492=CARTESIAN_POINT ( 'NONE',  ( 11.41020680648336771, 16.95828056793917682, 11.49999999999999645 ) ) ;
#72494=EDGE_CURVE ( 'NONE', #96725, #30324, #78418, .T. ) ;
#72496=ORIENTED_EDGE ( 'NONE', *, *, #70022, .F. ) ;
#72497=CARTESIAN_POINT ( 'NONE',  ( -59.62287095715004881, -29.50248528299804818, 1.056150453629034924 ) ) ;
#72500=CARTESIAN_POINT ( 'NONE',  ( -49.27881313098881577, -25.31439476491641472, 6.114505416649892666 ) ) ;
#72501=ADVANCED_FACE ( 'NONE', ( #93140 ), #71328, .T. ) ;
#72503=VERTEX_POINT ( 'NONE', #39368 ) ;
#72504=CARTESIAN_POINT ( 'NONE',  ( -66.60923601032587271, -23.48786465467241058, 11.44779295918254824 ) ) ;
#72506=EDGE_CURVE ( 'NONE', #14881, #26599, #76675, .T. ) ;
#72507=CARTESIAN_POINT ( 'NONE',  ( -21.12268324108725892, 9.058254180033936009, 11.49999999999999645 ) ) ;
#72508=CARTESIAN_POINT ( 'NONE',  ( -9.471985145535571249, 20.67137392225973258, -1.500000000000002220 ) ) ;
#72509=CARTESIAN_POINT ( 'NONE',  ( -110.5878943189815118, -24.73531770709095312, 8.716586749053508498 ) ) ;
#72510=B_SPLINE_SURFACE_WITH_KNOTS ( 'NONE', 3, 3, ( 
 ( #61137, #69231, #62631, #92064 ),
 ( #78326, #54020, #39769, #70734 ),
 ( #78822, #1228, #63134, #94060 ),
 ( #37784, #68738, #99656, #22533 ),
 ( #84948, #53526, #38274, #15432 ),
 ( #84449, #100147, #14931, #30668 ),
 ( #61637, #92557, #46394, #57024 ) ),
 .UNSPECIFIED., .F., .F., .F.,
 ( 4, 3, 4 ),
 ( 4, 4 ),
 ( 0.0004766839783816073282, 0.1029713700210892480, 0.2054660560637968925 ),
 ( 0.7396821597525450320, 0.7410361722979724730 ),
 .UNSPECIFIED. ) ;
#72513=AXIS2_PLACEMENT_3D ( 'NONE', #29142, #75309, #29642 ) ;
#72514=CARTESIAN_POINT ( 'NONE',  ( -70.52287095715006160, -24.92579138211020151, 1.929029949965661794 ) ) ;
#72516=CARTESIAN_POINT ( 'NONE',  ( -11.13288495942205536, 18.84158392345546318, -1.500000000000002220 ) ) ;
#72520=CARTESIAN_POINT ( 'NONE',  ( -99.16166289166534398, -25.31200570402560146, 5.311370725124462844 ) ) ;
#72521=ORIENTED_EDGE ( 'NONE', *, *, #26545, .F. ) ;
#72522=CARTESIAN_POINT ( 'NONE',  ( -19.81292649638395531, 4.959676026661640869, 11.49999999999998934 ) ) ;
#72525=CARTESIAN_POINT ( 'NONE',  ( 21.12055942831636202, -9.126644407798330860, 11.49999999999998934 ) ) ;
#72526=CARTESIAN_POINT ( 'NONE',  ( -80.52287095715007581, -23.48783264082477018, -1.443836473390091246 ) ) ;
#72527=ORIENTED_EDGE ( 'NONE', *, *, #17341, .T. ) ;
#72528=DIRECTION ( 'NONE',  ( -3.773278334444166432E-23, 1.000000000000000000, 0.000000000000000000 ) ) ;
#72530=DIRECTION ( 'NONE',  ( 1.000000000000000000, 3.773278334444167608E-23, 8.201307833595939069E-29 ) ) ;
#72532=CARTESIAN_POINT ( 'NONE',  ( -18.60337119584764665, 10.53494341765418874, 11.49999999999999645 ) ) ;
#72533=ORIENTED_EDGE ( 'NONE', *, *, #28553, .F. ) ;
#72534=ORIENTED_EDGE ( 'NONE', *, *, #67091, .F. ) ;
#72535=CARTESIAN_POINT ( 'NONE',  ( -18.24902840909259538, -12.68162010772806170, 11.49999999999998934 ) ) ;
#72536=CARTESIAN_POINT ( 'NONE',  ( 13.32396043830641830, 15.83023408377254704, -1.500000000000002220 ) ) ;
#72540=PLANE ( 'NONE',  #38195 ) ;
#72542=ORIENTED_EDGE ( 'NONE', *, *, #33507, .F. ) ;
#72543=CARTESIAN_POINT ( 'NONE',  ( -95.52287095715003318, -24.82558206586148941, 1.605769216559624457 ) ) ;
#72544=AXIS2_PLACEMENT_3D ( 'NONE', #79795, #26524, #81303 ) ;
#72545=EDGE_LOOP ( 'NONE', ( #65924, #14859, #69777, #14638 ) ) ;
#72547=CARTESIAN_POINT ( 'NONE',  ( -5.376107494350208960, -20.15860285114975525, -1.500000000000002220 ) ) ;
#72548=CARTESIAN_POINT ( 'NONE',  ( 9.607415760296678542, -19.69187540195887465, 11.49999999999999645 ) ) ;
#72551=CARTESIAN_POINT ( 'NONE',  ( 21.68943130245101258, -6.005725296444199834, -1.500000000000002220 ) ) ;
#72552=CARTESIAN_POINT ( 'NONE',  ( 13.87900837158347755, -15.70065903812341013, -1.500000000000002220 ) ) ;
#72553=CARTESIAN_POINT ( 'NONE',  ( -89.40841769935767047, -25.29749010697736367, 3.864033824493484204 ) ) ;
#72556=ORIENTED_EDGE ( 'NONE', *, *, #6112, .F. ) ;
#72557=ORIENTED_EDGE ( 'NONE', *, *, #83318, .T. ) ;
#72559=CARTESIAN_POINT ( 'NONE',  ( -52.58237442762383296, -24.51314013834315375, 0.6176544820404124003 ) ) ;
#72561=EDGE_CURVE ( 'NONE', #34684, #31278, #81680, .T. ) ;
#72562=CARTESIAN_POINT ( 'NONE',  ( -16.73372362409233105, 13.38858591273363174, -1.500000000000002220 ) ) ;
#72564=PLANE ( 'NONE',  #47266 ) ;
#72566=CARTESIAN_POINT ( 'NONE',  ( 10.44912437418449969, 18.32051524777507723, -1.500000000000002220 ) ) ;
#72567=CARTESIAN_POINT ( 'NONE',  ( -102.5228709571500900, -23.47593901973090524, -1.443836447538996648 ) ) ;
#72568=CARTESIAN_POINT ( 'NONE',  ( -92.52287095715006160, -24.65952944569304606, 1.056160979905700570 ) ) ;
#72569=CARTESIAN_POINT ( 'NONE',  ( -52.62287095715005592, -23.48783264082478794, -1.443836473390070596 ) ) ;
#72570=CARTESIAN_POINT ( 'NONE',  ( -101.5124433422946737, -24.34968618360934300, 0.1864209137778871928 ) ) ;
#72571=CARTESIAN_POINT ( 'NONE',  ( -107.5228709571500758, -24.65952944569304961, 1.056160979905704123 ) ) ;
#72572=CARTESIAN_POINT ( 'NONE',  ( 11.67614657018352453, 18.69773523334854914, -1.500000000000002220 ) ) ;
#72574=CARTESIAN_POINT ( 'NONE',  ( -116.5581106647310889, -23.48783264082478439, -1.443836473390061936 ) ) ;
#72576=CARTESIAN_POINT ( 'NONE',  ( -60.48528285801528170, -24.83618233451449697, 1.606449574219535936 ) ) ;
#72578=EDGE_CURVE ( 'NONE', #38855, #7487, #15518, .T. ) ;
#72579=EDGE_CURVE ( 'NONE', #59433, #50558, #30687, .T. ) ;
#72580=CARTESIAN_POINT ( 'NONE',  ( -29.84334126970346190, -25.10778653237075275, 7.214475432169975555 ) ) ;
#72581=B_SPLINE_CURVE_WITH_KNOTS ( 'NONE', 3,
 ( #5209, #67132, #64272, #74226 ),
 .UNSPECIFIED., .F., .F.,
 ( 4, 4 ),
 ( 0.000000000000000000, 1.000000000000000000 ),
 .UNSPECIFIED. ) ;
#72582=CARTESIAN_POINT ( 'NONE',  ( -27.24386298623018021, -24.58417960884006348, 1.680793441616425410 ) ) ;
#72584=CARTESIAN_POINT ( 'NONE',  ( -56.58953762381672448, -23.48783264082478084, -1.443836473390068820 ) ) ;
#72585=CARTESIAN_POINT ( 'NONE',  ( -3.453506354162970915, -21.03206338698385736, 11.49999999999998934 ) ) ;
#72586=DIRECTION ( 'NONE',  ( -3.773278334453079030E-23, 0.9999999999976377785, 2.173523156925978705E-06 ) ) ;
#72587=CARTESIAN_POINT ( 'NONE',  ( -66.62287095715004170, -23.72747288104469376, -1.053458166803226348 ) ) ;
#72588=CARTESIAN_POINT ( 'NONE',  ( -64.57975408571323328, -24.66019654487199730, 8.947790411086115725 ) ) ;
#72589=CARTESIAN_POINT ( 'NONE',  ( -67.55620429048336462, -24.66019654487199020, 8.947790411086131712 ) ) ;
#72590=CARTESIAN_POINT ( 'NONE',  ( 19.13181028273733375, 12.02906595412573232, -1.500000000000002220 ) ) ;
#72591=B_SPLINE_SURFACE_WITH_KNOTS ( 'NONE', 3, 3, ( 
 ( #40958, #35350, #71919, #26230 ),
 ( #95241, #33331, #34846, #42966 ),
 ( #64323, #73902, #57204, #65815 ),
 ( #89132, #88138, #49581, #80514 ),
 ( #11006, #72915, #97240, #57692 ),
 ( #3413, #34348, #4401, #19107 ),
 ( #65326, #81019, #11497, #96737 ) ),
 .UNSPECIFIED., .F., .F., .F.,
 ( 4, 3, 4 ),
 ( 4, 4 ),
 ( 0.7945040073713779405, 0.8970133732236067470, 0.9995227390758355535 ),
 ( 0.03212669907356750093, 0.03698063968062436507 ),
 .UNSPECIFIED. ) ;
#72592=CARTESIAN_POINT ( 'NONE',  ( -112.5228709571500616, -23.47593901973090524, -1.443836447538996426 ) ) ;
#72594=CARTESIAN_POINT ( 'NONE',  ( -35.62287095715005592, -24.63345952396256777, 9.038047939301515399 ) ) ;
#72595=CARTESIAN_POINT ( 'NONE',  ( -120.5895376238167103, -23.47596703998600631, 11.44779298504227683 ) ) ;
#72596=CARTESIAN_POINT ( 'NONE',  ( 19.74453702311487646, -0.1846442961375113490, 11.49999999999999645 ) ) ;
#72597=CARTESIAN_POINT ( 'NONE',  ( -32.07722060962684196, -25.34389491264532879, 4.638595615756661239 ) ) ;
#72601=CARTESIAN_POINT ( 'NONE',  ( -42.52287095715005449, -23.47593901973090169, -1.443836447538997092 ) ) ;
#72602=CARTESIAN_POINT ( 'NONE',  ( -124.4728709571500360, -25.40675522342680637, 5.000950440042752021 ) ) ;
#72603=CARTESIAN_POINT ( 'NONE',  ( -124.5895423235921271, -24.35071581493544457, 9.817618358456016381 ) ) ;
#72608=CARTESIAN_POINT ( 'NONE',  ( -15.39140670439391378, -12.39996395878027791, 11.49999999999998934 ) ) ;
#72609=VERTEX_POINT ( 'NONE', #65733 ) ;
#72610=CARTESIAN_POINT ( 'NONE',  ( -9.470923242388245455, -17.85692771776473364, 11.49999999999999645 ) ) ;
#72611=CARTESIAN_POINT ( 'NONE',  ( -112.6228709571500559, -23.73934037231757799, 11.05740245334328975 ) ) ;
#72612=EDGE_CURVE ( 'NONE', #40589, #98594, #63535, .T. ) ;
#72614=EDGE_CURVE ( 'NONE', #51996, #94218, #8953, .T. ) ;
#72618=CARTESIAN_POINT ( 'NONE',  ( -59.55620429048338593, -23.48786465467241058, 11.44779295918255180 ) ) ;
#72619=CARTESIAN_POINT ( 'NONE',  ( -31.55620429048338593, -23.48786465467240347, 11.44779295918255002 ) ) ;
#72620=VECTOR ( 'NONE', #1278, 1000.000000000000114 ) ;
#72621=LINE ( 'NONE', #42183, #86180 ) ;
#72622=CARTESIAN_POINT ( 'NONE',  ( -58.55620429048339304, -24.64898659630528144, 1.056161002820823036 ) ) ;
#72623=CARTESIAN_POINT ( 'NONE',  ( 15.84714387567644955, -12.28532832577633194, 11.49999999999998934 ) ) ;
#72624=ADVANCED_FACE ( 'NONE', ( #59109 ), #36261, .F. ) ;
#72625=DIRECTION ( 'NONE',  ( 1.000000000000000000, 3.773278334444166432E-23, 8.201307841325785021E-29 ) ) ;
#72626=ORIENTED_EDGE ( 'NONE', *, *, #88042, .T. ) ;
#72627=EDGE_CURVE ( 'NONE', #84363, #9929, #44881, .T. ) ;
#72631=B_SPLINE_CURVE_WITH_KNOTS ( 'NONE', 3,
 ( #61652, #92078, #92570, #15449 ),
 .UNSPECIFIED., .F., .F.,
 ( 4, 4 ),
 ( 0.000000000000000000, 9.999999999999592548E-05 ),
 .UNSPECIFIED. ) ;
#72632=CARTESIAN_POINT ( 'NONE',  ( -96.62287095715005592, -24.64898659630368272, 1.056161002820829697 ) ) ;
#72633=CARTESIAN_POINT ( 'NONE',  ( -79.44752152392706535, -25.29575941214698531, 5.495406740378385280 ) ) ;
#72634=LINE ( 'NONE', #3126, #98370 ) ;
#72635=CARTESIAN_POINT ( 'NONE',  ( -73.53861189177032998, -24.65952944569304606, 1.056160979905700126 ) ) ;
#72637=EDGE_CURVE ( 'NONE', #45965, #45491, #71987, .T. ) ;
#72638=CARTESIAN_POINT ( 'NONE',  ( -49.51010171462829135, -25.25846184752573720, 3.931802542169027248 ) ) ;
#72639=VERTEX_POINT ( 'NONE', #67225 ) ;
#72640=CARTESIAN_POINT ( 'NONE',  ( -18.18203184671642703, 9.085611141607108365, 11.49999999999998934 ) ) ;
#72641=VERTEX_POINT ( 'NONE', #29636 ) ;
#72642=FACE_OUTER_BOUND ( 'NONE', #62457, .T. ) ;
#72643=CARTESIAN_POINT ( 'NONE',  ( -127.5222628862546514, -23.48786465467242124, 11.44779295918253226 ) ) ;
#72645=CARTESIAN_POINT ( 'NONE',  ( -105.6228709571501128, -24.15431212366391378, -0.2830839119428946726 ) ) ;
#72646=CARTESIAN_POINT ( 'NONE',  ( -49.29494865489761679, -25.12215252155673895, 6.331091545398378706 ) ) ;
#72648=CARTESIAN_POINT ( 'NONE',  ( -9.361133326760958440, -19.03884994183470880, 11.49999999999999645 ) ) ;
#72649=CARTESIAN_POINT ( 'NONE',  ( -10.67647856527443473, 19.39090429279614369, 11.49999999999998934 ) ) ;
#72650=CARTESIAN_POINT ( 'NONE',  ( 14.24201292913401140, 14.87178044790754328, 11.49999999999998934 ) ) ;
#72652=CARTESIAN_POINT ( 'NONE',  ( -41.53391078925199764, -24.51314013834315375, 0.6176544820404115121 ) ) ;
#72657=ORIENTED_EDGE ( 'NONE', *, *, #87049, .F. ) ;
#72658=ORIENTED_EDGE ( 'NONE', *, *, #41023, .T. ) ;
#72659=CARTESIAN_POINT ( 'NONE',  ( -116.6228709571500275, -24.33927499327854704, 9.819080762295804732 ) ) ;
#72662=CARTESIAN_POINT ( 'NONE',  ( 19.89799572200132971, -5.707369160466581270, -1.500000000000002220 ) ) ;
#72663=CARTESIAN_POINT ( 'NONE',  ( 7.043455336710909620, -20.48365140995157674, 11.49999999999999645 ) ) ;
#72666=CARTESIAN_POINT ( 'NONE',  ( -110.7976466536441080, -25.12311862853486133, 2.903749597397971449 ) ) ;
#72667=CARTESIAN_POINT ( 'NONE',  ( -9.774569144048079750, -20.17623354167628946, 11.49999999999998934 ) ) ;
#72670=CARTESIAN_POINT ( 'NONE',  ( -65.52204162676289911, -23.48783264082477018, -1.443836473390096353 ) ) ;
#72671=ORIENTED_EDGE ( 'NONE', *, *, #70732, .T. ) ;
#72674=ORIENTED_EDGE ( 'NONE', *, *, #20047, .F. ) ;
#72675=EDGE_LOOP ( 'NONE', ( #81036, #3174, #85008, #70005 ) ) ;
#72677=ORIENTED_EDGE ( 'NONE', *, *, #29248, .F. ) ;
#72678=DIRECTION ( 'NONE',  ( 0.000000000000000000, 0.9999999999976377785, 2.173523156925979975E-06 ) ) ;
#72680=CARTESIAN_POINT ( 'NONE',  ( 13.55612473118199723, -16.30799122071102403, -1.500000000000002220 ) ) ;
#72681=EDGE_LOOP ( 'NONE', ( #10771, #18908, #61410, #79080 ) ) ;
#72682=CARTESIAN_POINT ( 'NONE',  ( -68.62287095715008434, -24.51283580621364067, 0.6167428607019829201 ) ) ;
#72684=CARTESIAN_POINT ( 'NONE',  ( -9.754611696910345131, 19.53525426502628548, -1.500000000000002220 ) ) ;
#72685=CARTESIAN_POINT ( 'NONE',  ( -103.5172066925842103, -23.96169478059713498, 10.65365249895717881 ) ) ;
#72688=CARTESIAN_POINT ( 'NONE',  ( -35.62287095715002749, -24.51163499207174468, 0.6490370598554239256 ) ) ;
#72689=CARTESIAN_POINT ( 'NONE',  ( -11.18773875818744656, -18.78983145652188469, -1.500000000000002220 ) ) ;
#72691=ORIENTED_EDGE ( 'NONE', *, *, #62184, .T. ) ;
#72696=ORIENTED_EDGE ( 'NONE', *, *, #34577, .T. ) ;
#72701=DIRECTION ( 'NONE',  ( -0.000000000000000000, 2.173523156925979552E-06, -0.9999999999976378895 ) ) ;
#72702=EDGE_CURVE ( 'NONE', #14136, #72949, #48982, .T. ) ;
#72703=CARTESIAN_POINT ( 'NONE',  ( -79.11611000704996854, -25.21083105912962097, 3.409327675794633361 ) ) ;
#72704=CARTESIAN_POINT ( 'NONE',  ( 6.411417644607832145, 20.24884965431308714, 11.49999999999998934 ) ) ;
#72706=CARTESIAN_POINT ( 'NONE',  ( -130.5728709571500588, -23.56000036390796737, 11.50200000000000244 ) ) ;
#72708=CARTESIAN_POINT ( 'NONE',  ( -68.49733487582329872, -24.51314013834315375, 0.6176544820404119562 ) ) ;
#72709=CARTESIAN_POINT ( 'NONE',  ( -19.08929872761019908, -3.557156390981079053, 11.49999999999998934 ) ) ;
#72710=CARTESIAN_POINT ( 'NONE',  ( -45.52798609474427138, -24.83618233451449697, 1.606449574219536158 ) ) ;
#72712=CARTESIAN_POINT ( 'NONE',  ( 10.47639735327893362, 16.54961352017854637, 11.49999999999999645 ) ) ;
#72716=ORIENTED_EDGE ( 'NONE', *, *, #85996, .F. ) ;
#72718=CARTESIAN_POINT ( 'NONE',  ( -75.62287095715004170, -24.63287334234180292, 0.9662140553045361901 ) ) ;
#72721=CARTESIAN_POINT ( 'NONE',  ( 19.69511366699831001, -0.05742560045514189665, -1.500000000000002220 ) ) ;
#72724=LINE ( 'NONE', #41269, #95905 ) ;
#72725=CARTESIAN_POINT ( 'NONE',  ( -0.07435467474217070938, 23.09247799282200475, -1.500000000000002220 ) ) ;
#72726=EDGE_CURVE ( 'NONE', #56862, #4409, #2978, .T. ) ;
#72731=LINE ( 'NONE', #31280, #26450 ) ;
#72732=PLANE ( 'NONE',  #78457 ) ;
#72736=CARTESIAN_POINT ( 'NONE',  ( -69.45824367449309023, -25.24515144706554182, 5.785093357820605853 ) ) ;
#72737=B_SPLINE_CURVE_WITH_KNOTS ( 'NONE', 3,
 ( #6513, #68413, #92730, #62821, #23217, #38456 ),
 .UNSPECIFIED., .F., .F.,
 ( 4, 2, 4 ),
 ( 0.000000000000000000, 0.001380764517854760412, 0.002761529035709520824 ),
 .UNSPECIFIED. ) ;
#72739=CARTESIAN_POINT ( 'NONE',  ( 19.82558669001425500, -2.195561414069463702, -1.500000000000002220 ) ) ;
#72740=CARTESIAN_POINT ( 'NONE',  ( -75.49535866980721721, -24.73531770709095312, 8.716586749053512051 ) ) ;
#72741=CARTESIAN_POINT ( 'NONE',  ( 18.24224480919323810, -7.949361806615760528, -1.500000000000002220 ) ) ;
#72743=AXIS2_PLACEMENT_3D ( 'NONE', #8004, #61809, #93734 ) ;
#72744=CARTESIAN_POINT ( 'NONE',  ( -111.5228709571500616, -29.50247984919015209, -1.443849546365048253 ) ) ;
#72745=ADVANCED_FACE ( 'NONE', ( #44378 ), #23000, .F. ) ;
#72747=CARTESIAN_POINT ( 'NONE',  ( -72.58953762381672448, -24.64898659630367916, 1.056161002820384942 ) ) ;
#72749=CARTESIAN_POINT ( 'NONE',  ( -18.04518632387085830, 10.29925911722504317, 11.49999999999999645 ) ) ;
#72751=VECTOR ( 'NONE', #69242, 1000.000000000000227 ) ;
#72754=CARTESIAN_POINT ( 'NONE',  ( 22.56601425305882813, -3.627385684441148506, 11.49999999999999645 ) ) ;
#72755=ORIENTED_EDGE ( 'NONE', *, *, #925, .T. ) ;
#72756=CARTESIAN_POINT ( 'NONE',  ( -108.6228709571500559, -24.64965695001468404, 8.947790433994176951 ) ) ;
#72757=DIRECTION ( 'NONE',  ( 3.773278334444167020E-23, -1.000000000000000000, 0.000000000000000000 ) ) ;
#72758=ORIENTED_EDGE ( 'NONE', *, *, #92864, .T. ) ;
#72759=VECTOR ( 'NONE', #8093, 1000.000000000000114 ) ;
#72760=CARTESIAN_POINT ( 'NONE',  ( 20.02926185082240451, -2.967945350358753398, -1.500000000000002220 ) ) ;
#72765=ORIENTED_EDGE ( 'NONE', *, *, #59686, .F. ) ;
#72766=CARTESIAN_POINT ( 'NONE',  ( -80.35919894935766195, -25.30543142107805465, 4.505481316334992492 ) ) ;
#72768=CARTESIAN_POINT ( 'NONE',  ( 12.72590371223024697, 15.41468647733915809, -1.500000000000002220 ) ) ;
#72769=B_SPLINE_CURVE_WITH_KNOTS ( 'NONE', 3,
 ( #19395, #40742, #10292, #3692 ),
 .UNSPECIFIED., .F., .F.,
 ( 4, 4 ),
 ( 0.000000000000000000, 0.0001000000000000444977 ),
 .UNSPECIFIED. ) ;
#72770=CARTESIAN_POINT ( 'NONE',  ( 17.97375762979478253, -10.76934015532128797, 11.49999999999999645 ) ) ;
#72773=CARTESIAN_POINT ( 'NONE',  ( 15.63414672909509839, 15.54323407889855879, 11.49999999999998934 ) ) ;
#72775=ORIENTED_EDGE ( 'NONE', *, *, #73135, .T. ) ;
#72776=DIRECTION ( 'NONE',  ( -3.773278334453079618E-23, 0.9999999999976377785, 2.173523156925979975E-06 ) ) ;
#72777=PLANE ( 'NONE',  #37926 ) ;
#72779=CARTESIAN_POINT ( 'NONE',  ( -31.62374191384759925, -24.65952944569304250, 1.056160979905695463 ) ) ;
#72780=VERTEX_POINT ( 'NONE', #92526 ) ;
#72782=CARTESIAN_POINT ( 'NONE',  ( -118.5562042904834072, -24.66019654487199730, 8.947790411086121054 ) ) ;
#72783=CARTESIAN_POINT ( 'NONE',  ( -100.4381051993576506, -25.10935802465470701, 2.832404819424185316 ) ) ;
#72784=DIRECTION ( 'NONE',  ( 0.000000000000000000, 2.173523156925980399E-06, -0.9999999999976378895 ) ) ;
#72785=CARTESIAN_POINT ( 'NONE',  ( -17.09319154528168383, -11.34935287704045948, -1.500000000000002220 ) ) ;
#72786=ORIENTED_EDGE ( 'NONE', *, *, #97973, .T. ) ;
#72790=CARTESIAN_POINT ( 'NONE',  ( 18.98964132805693694, -11.70494588174365092, 11.49999999999998934 ) ) ;
#72791=CARTESIAN_POINT ( 'NONE',  ( -0.05753151201984623569, -22.30520936630598072, 1.095224832288517858 ) ) ;
#72792=ORIENTED_EDGE ( 'NONE', *, *, #89659, .T. ) ;
#72793=CARTESIAN_POINT ( 'NONE',  ( -101.6228709571500559, -24.51283580621365132, 0.6167428607019800335 ) ) ;
#72795=CARTESIAN_POINT ( 'NONE',  ( 11.47802407633690258, -17.41396394059345454, 11.49999999999998934 ) ) ;
#72796=ORIENTED_EDGE ( 'NONE', *, *, #19918, .T. ) ;
#72798=ORIENTED_EDGE ( 'NONE', *, *, #58250, .F. ) ;
#72799=VERTEX_POINT ( 'NONE', #31128 ) ;
#72801=CARTESIAN_POINT ( 'NONE',  ( 18.24537196375281312, 10.48796402029766739, -1.500000000000002220 ) ) ;
#72802=EDGE_CURVE ( 'NONE', #59928, #8232, #62102, .T. ) ;
#72803=VERTEX_POINT ( 'NONE', #85415 ) ;
#72805=AXIS2_PLACEMENT_3D ( 'NONE', #98196, #66791, #36817 ) ;
#72806=CARTESIAN_POINT ( 'NONE',  ( -37.52287095715006870, -24.50321055353803601, 9.387540953477520489 ) ) ;
#72807=EDGE_CURVE ( 'NONE', #40031, #19500, #77293, .T. ) ;
#72809=VECTOR ( 'NONE', #59340, 1000.000000000000114 ) ;
#72811=CARTESIAN_POINT ( 'NONE',  ( -101.9195342205254775, -25.03152194789300822, 6.392810880780148253 ) ) ;
#72813=CARTESIAN_POINT ( 'NONE',  ( 7.679218611123722837, 20.28660689097963399, -1.500000000000002220 ) ) ;
#72814=CARTESIAN_POINT ( 'NONE',  ( -81.48149462243461016, -25.24759629374391423, 6.293942980506744611 ) ) ;
#72815=CARTESIAN_POINT ( 'NONE',  ( 14.93699691249320693, 16.48547057857716425, 11.49999999999999645 ) ) ;
#72816=ORIENTED_EDGE ( 'NONE', *, *, #90792, .T. ) ;
#72817=CARTESIAN_POINT ( 'NONE',  ( -51.52657066994672164, -25.24728931607062776, 6.155056572741268717 ) ) ;
#72818=CARTESIAN_POINT ( 'NONE',  ( -105.5228709571500758, -23.47593901973090524, -1.443836447538996426 ) ) ;
#72821=EDGE_CURVE ( 'NONE', #6511, #57950, #70703, .T. ) ;
#72822=B_SPLINE_CURVE_WITH_KNOTS ( 'NONE', 3,
 ( #93049, #30160, #61134, #54508 ),
 .UNSPECIFIED., .F., .F.,
 ( 4, 4 ),
 ( 2.796599675949392459E-06, 0.0004696118376083021489 ),
 .UNSPECIFIED. ) ;
#72824=ADVANCED_FACE ( 'NONE', ( #684 ), #39242, .T. ) ;
#72826=ORIENTED_EDGE ( 'NONE', *, *, #35575, .F. ) ;
#72827=AXIS2_PLACEMENT_3D ( 'NONE', #43454, #11987, #35830 ) ;
#72828=EDGE_LOOP ( 'NONE', ( #1807, #96532, #31990, #57413 ) ) ;
#72831=CARTESIAN_POINT ( 'NONE',  ( -107.5228709571501042, -24.51283580621451108, 0.6167428607045601918 ) ) ;
#72833=ORIENTED_EDGE ( 'NONE', *, *, #54260, .F. ) ;
#72834=CARTESIAN_POINT ( 'NONE',  ( -130.5728709571500588, -25.32188240763692733, 6.439777313841902107 ) ) ;
#72835=CARTESIAN_POINT ( 'NONE',  ( -0.1411031551986380028, 22.44022050402121948, -1.500000000000002220 ) ) ;
#72836=ORIENTED_EDGE ( 'NONE', *, *, #20583, .T. ) ;
#72837=CARTESIAN_POINT ( 'NONE',  ( -108.8968792378191921, -29.50249917535260380, 7.447779886225679213 ) ) ;
#72838=CARTESIAN_POINT ( 'NONE',  ( -44.92287095715006018, -23.47593901973090169, -1.443836447538997980 ) ) ;
#72839=DIRECTION ( 'NONE',  ( 0.000000000000000000, 2.173523156925980399E-06, -0.9999999999976378895 ) ) ;
#72841=CARTESIAN_POINT ( 'NONE',  ( -97.24175110560238977, -25.14081846633248318, 7.291654623549835179 ) ) ;
#72842=CARTESIAN_POINT ( 'NONE',  ( 12.01011565470214393, -15.49198969801113890, -1.500000000000002220 ) ) ;
#72845=CARTESIAN_POINT ( 'NONE',  ( -7.320277434469578459, 20.25297033093062282, 11.49999999999998934 ) ) ;
#72847=CARTESIAN_POINT ( 'NONE',  ( -80.53911428444936860, -25.30394759708685015, 4.969307535586566793 ) ) ;
#72849=CARTESIAN_POINT ( 'NONE',  ( -41.86995616089613748, -29.50249213948574933, 4.210700559310249780 ) ) ;
#72850=CARTESIAN_POINT ( 'NONE',  ( 16.30191990219073972, -16.09819076282585826, -1.500000000000002220 ) ) ;
#72851=B_SPLINE_CURVE_WITH_KNOTS ( 'NONE', 3,
 ( #98375, #97394, #5042, #34996 ),
 .UNSPECIFIED., .F., .F.,
 ( 4, 4 ),
 ( 3.316619621408722944E-09, 0.002461457897985275343 ),
 .UNSPECIFIED. ) ;
#72855=CARTESIAN_POINT ( 'NONE',  ( -11.83016301840747175, -16.26703346747452983, 11.49999999999999645 ) ) ;
#72857=CARTESIAN_POINT ( 'NONE',  ( -32.59411303382088931, -24.15620529776627734, 10.23563542870661358 ) ) ;
#72858=B_SPLINE_CURVE_WITH_KNOTS ( 'NONE', 3,
 ( #57648, #48540, #94688, #72868, #9957, #87078 ),
 .UNSPECIFIED., .F., .F.,
 ( 4, 2, 4 ),
 ( 0.000000000000000000, 0.001380764517854768001, 0.002761529035709536003 ),
 .UNSPECIFIED. ) ;
#72862=CARTESIAN_POINT ( 'NONE',  ( -19.21288746854601115, 4.878285775029977955, 11.49999999999998934 ) ) ;
#72863=B_SPLINE_CURVE_WITH_KNOTS ( 'NONE', 3,
 ( #79443, #11437, #71848, #2845, #58619, #3351 ),
 .UNSPECIFIED., .F., .F.,
 ( 4, 2, 4 ),
 ( 1.570887131794638196E-05, 0.001396322306279761940, 0.002776935741241577573 ),
 .UNSPECIFIED. ) ;
#72864=CARTESIAN_POINT ( 'NONE',  ( -90.62287095715001328, -24.63345952396257843, 9.038047939301508293 ) ) ;
#72865=CARTESIAN_POINT ( 'NONE',  ( -9.297559507673007317, 17.40068379117045083, -1.500000000000002220 ) ) ;
#72868=CARTESIAN_POINT ( 'NONE',  ( -103.5228709571500758, -23.94994826722565406, -0.6494450866342691420 ) ) ;
#72870=CARTESIAN_POINT ( 'NONE',  ( 17.30552477474510908, -11.17933342135444086, 11.49999999999999645 ) ) ;
#72872=EDGE_CURVE ( 'NONE', #84333, #23301, #17519, .T. ) ;
#72873=CARTESIAN_POINT ( 'NONE',  ( -116.6228709571500559, -29.50250243563736774, 8.947779886222134493 ) ) ;
#72874=CARTESIAN_POINT ( 'NONE',  ( 12.64511023617726160, -18.80563239904246231, 11.49999999999999645 ) ) ;
#72875=ORIENTED_EDGE ( 'NONE', *, *, #58225, .T. ) ;
#72877=CARTESIAN_POINT ( 'NONE',  ( -69.35973275182155362, -25.25639446185967785, 6.387116080414448227 ) ) ;
#72879=AXIS2_PLACEMENT_3D ( 'NONE', #100048, #75723, #22922 ) ;
#72880=CARTESIAN_POINT ( 'NONE',  ( -27.55559746109228669, -24.61460113352056567, 8.249645512891413901 ) ) ;
#72881=CARTESIAN_POINT ( 'NONE',  ( -36.52287095715006870, -23.48783264082477018, -1.443836473390097019 ) ) ;
#72883=ORIENTED_EDGE ( 'NONE', *, *, #30405, .T. ) ;
#72884=CARTESIAN_POINT ( 'NONE',  ( -79.98791220707269645, -25.31596236519360588, 5.033164519372586021 ) ) ;
#72885=CARTESIAN_POINT ( 'NONE',  ( -21.74551633039419585, 6.958787177381512201, 11.49999999999998934 ) ) ;
#72889=CARTESIAN_POINT ( 'NONE',  ( -82.55439147425074964, -23.96169478059713143, 10.65365249895718414 ) ) ;
#72890=CARTESIAN_POINT ( 'NONE',  ( -16.74552829020559130, -14.98668287627115170, 11.49999999999999645 ) ) ;
#72891=ORIENTED_EDGE ( 'NONE', *, *, #65079, .T. ) ;
#72892=AXIS2_PLACEMENT_3D ( 'NONE', #48772, #96930, #18799 ) ;
#72893=B_SPLINE_CURVE_WITH_KNOTS ( 'NONE', 3,
 ( #99895, #85701, #7572, #69474 ),
 .UNSPECIFIED., .F., .F.,
 ( 4, 4 ),
 ( 0.000000000000000000, 9.999999999998897304E-05 ),
 .UNSPECIFIED. ) ;
#72894=CARTESIAN_POINT ( 'NONE',  ( -69.55126625704997423, -25.15208592601422311, 3.076695591939294427 ) ) ;
#72895=CARTESIAN_POINT ( 'NONE',  ( -19.44315311050126382, -10.23602577120861667, -1.500000000000002220 ) ) ;
#72896=CARTESIAN_POINT ( 'NONE',  ( -125.5801350442859246, -25.31825869351653679, 3.539998670762456889 ) ) ;
#72897=AXIS2_PLACEMENT_3D ( 'NONE', #69173, #100093, #30607 ) ;
#72898=CARTESIAN_POINT ( 'NONE',  ( -111.5146153425688169, -24.51314013834316796, 0.6176544820404207270 ) ) ;
#72899=PLANE ( 'NONE',  #83206 ) ;
#72901=CARTESIAN_POINT ( 'NONE',  ( -48.56838548480330076, -23.48786465467241058, 11.44779295918254824 ) ) ;
#72902=FACE_OUTER_BOUND ( 'NONE', #71031, .T. ) ;
#72903=ORIENTED_EDGE ( 'NONE', *, *, #68919, .T. ) ;
#72904=CARTESIAN_POINT ( 'NONE',  ( -54.53280603000485627, -24.66019654487199375, 8.947790411086119278 ) ) ;
#72905=CARTESIAN_POINT ( 'NONE',  ( -14.05295919346176170, -14.94737400546395456, -1.500000000000002220 ) ) ;
#72907=ORIENTED_EDGE ( 'NONE', *, *, #23050, .T. ) ;
#72908=ORIENTED_EDGE ( 'NONE', *, *, #17189, .T. ) ;
#72910=CARTESIAN_POINT ( 'NONE',  ( 8.286623624103266097E-13, -23.05000000000000426, -1.500000000000002220 ) ) ;
#72912=CARTESIAN_POINT ( 'NONE',  ( 10.94010344783756672, -17.16519937159427656, -1.500000000000002220 ) ) ;
#72913=ORIENTED_EDGE ( 'NONE', *, *, #50775, .F. ) ;
#72915=CARTESIAN_POINT ( 'NONE',  ( -29.60196408342335772, -23.88237758481870188, 10.65365256123546978 ) ) ;
#72917=CARTESIAN_POINT ( 'NONE',  ( -105.5543693429755052, -24.15503026093913519, -0.2815557561904565298 ) ) ;
#72918=CARTESIAN_POINT ( 'NONE',  ( -71.70602904702231228, -25.25855097290165574, 6.253518357416208318 ) ) ;
#72920=CARTESIAN_POINT ( 'NONE',  ( -29.19847332116389538, -25.21532038932136643, 4.026235508823390319 ) ) ;
#72921=CARTESIAN_POINT ( 'NONE',  ( -49.59506520832605503, -25.31573813936321216, 4.856709705808007982 ) ) ;
#72922=VERTEX_POINT ( 'NONE', #16399 ) ;
#72923=CARTESIAN_POINT ( 'NONE',  ( -2.730994233912177549, 20.60462238790213618, -1.500000000000002220 ) ) ;
#72924=ORIENTED_EDGE ( 'NONE', *, *, #93546, .T. ) ;
#72925=CARTESIAN_POINT ( 'NONE',  ( -39.64514910329782538, -25.30345942151094007, 4.760327011971625666 ) ) ;
#72929=ORIENTED_EDGE ( 'NONE', *, *, #56483, .T. ) ;
#72930=ORIENTED_EDGE ( 'NONE', *, *, #89197, .T. ) ;
#72931=CARTESIAN_POINT ( 'NONE',  ( -77.62287095715005592, -29.50250786944525672, 11.44777988621623521 ) ) ;
#72933=PLANE ( 'NONE',  #52991 ) ;
#72934=CARTESIAN_POINT ( 'NONE',  ( -71.15736797201716968, -25.31201676987124927, 5.711157391728908017 ) ) ;
#72935=CARTESIAN_POINT ( 'NONE',  ( 21.54648482299927181, -4.703075207800759827, 11.49999999999999645 ) ) ;
#72936=VERTEX_POINT ( 'NONE', #63103 ) ;
#72937=CARTESIAN_POINT ( 'NONE',  ( -50.52287095715007581, -25.00182538069144655, 7.747789668545104647 ) ) ;
#72939=CARTESIAN_POINT ( 'NONE',  ( 19.13181028273733375, 12.02906595412573232, 11.49999999999998934 ) ) ;
#72940=EDGE_CURVE ( 'NONE', #21005, #53793, #67130, .T. ) ;
#72941=CARTESIAN_POINT ( 'NONE',  ( -70.62287095715005592, -24.14321612903114556, -0.2833117244521698996 ) ) ;
#72942=VERTEX_POINT ( 'NONE', #32130 ) ;
#72946=DIRECTION ( 'NONE',  ( 0.000000000000000000, -2.173523156925979552E-06, 0.9999999999976378895 ) ) ;
#72948=CARTESIAN_POINT ( 'NONE',  ( -36.52287095715006870, -24.64965694238407323, 8.947790433994205372 ) ) ;
#72949=VERTEX_POINT ( 'NONE', #42283 ) ;
#72950=CARTESIAN_POINT ( 'NONE',  ( -1.756177585742932479, 21.11346882147791959, -1.500000000000002220 ) ) ;
#72951=CARTESIAN_POINT ( 'NONE',  ( -78.97085663747836293, -25.27791698645071250, 6.301135832498177436 ) ) ;
#72954=CARTESIAN_POINT ( 'NONE',  ( -39.62287095715005592, -23.47593901973091235, -1.443836447539011525 ) ) ;
#72955=CARTESIAN_POINT ( 'NONE',  ( -8.951960448472247478, 20.35530821588910300, -1.500000000000002220 ) ) ;
#72956=CARTESIAN_POINT ( 'NONE',  ( -49.32147450118114307, -25.03220824940797584, 7.186702319186736965 ) ) ;
#72958=ORIENTED_EDGE ( 'NONE', *, *, #29005, .F. ) ;
#72962=CARTESIAN_POINT ( 'NONE',  ( -36.64924296586449515, -23.96169478059712432, 10.65365249895718591 ) ) ;
#72965=CARTESIAN_POINT ( 'NONE',  ( -12.17249226084429203, 15.20430173202493940, 11.49999999999998934 ) ) ;
#72966=VECTOR ( 'NONE', #81629, 1000.000000000000114 ) ;
#72967=CARTESIAN_POINT ( 'NONE',  ( 21.15477495681221143, 3.540436534888726783, 11.49999999999998934 ) ) ;
#72968=CARTESIAN_POINT ( 'NONE',  ( -27.26447433122779884, -24.57999507273727247, 1.676005322195218916 ) ) ;
#72969=CARTESIAN_POINT ( 'NONE',  ( -51.48601377777728771, -24.65952944569304250, 1.056160979905695463 ) ) ;
#72970=CARTESIAN_POINT ( 'NONE',  ( -77.62998606892628572, -24.34968618360934300, 0.1864209137778811143 ) ) ;
#72971=B_SPLINE_CURVE_WITH_KNOTS ( 'NONE', 3,
 ( #27646, #65728, #13892, #43376 ),
 .UNSPECIFIED., .F., .F.,
 ( 4, 4 ),
 ( 0.000000000000000000, 1.000000000000000000 ),
 .UNSPECIFIED. ) ;
#72972=CARTESIAN_POINT ( 'NONE',  ( -2.780358639097238349, 22.57001311929844434, -1.500000000000002220 ) ) ;
#72973=B_SPLINE_CURVE_WITH_KNOTS ( 'NONE', 3,
 ( #90144, #66331, #20620, #27747, #58697, #57711 ),
 .UNSPECIFIED., .F., .F.,
 ( 4, 2, 4 ),
 ( 0.000000000000000000, 0.001380901958385383774, 0.002761803916770767548 ),
 .UNSPECIFIED. ) ;
#72974=VECTOR ( 'NONE', #15895, 1000.000000000000114 ) ;
#72976=CARTESIAN_POINT ( 'NONE',  ( -102.5221945332385758, -23.48783264082478084, -1.443836473390064379 ) ) ;
#72977=CARTESIAN_POINT ( 'NONE',  ( -88.52287095715006160, -29.50247984919015209, -1.443849546365051806 ) ) ;
#72978=CARTESIAN_POINT ( 'NONE',  ( 4.721227339208565965, -19.33841413273825793, 11.49999999999999645 ) ) ;
#72979=LINE ( 'NONE', #57268, #34070 ) ;
#72980=CARTESIAN_POINT ( 'NONE',  ( -39.49832869534071733, -24.15620529776627734, 10.23563542870661180 ) ) ;
#72985=CARTESIAN_POINT ( 'NONE',  ( -32.40928876965531913, -25.16202561908117730, 2.791798636425737445 ) ) ;
#72986=CARTESIAN_POINT ( 'NONE',  ( 19.26462925850498920, -9.998780574493274287, -1.500000000000002220 ) ) ;
#72988=CARTESIAN_POINT ( 'NONE',  ( -4.924063254364682507, -18.92933890202812464, -1.500000000000002220 ) ) ;
#72994=CARTESIAN_POINT ( 'NONE',  ( -4.302178748239556150, -20.00421716419250373, 11.49999999999999645 ) ) ;
#72995=CARTESIAN_POINT ( 'NONE',  ( -82.62287095715005592, -23.48783264082478084, -1.443836473390065933 ) ) ;
#72996=EDGE_CURVE ( 'NONE', #18460, #75143, #44118, .T. ) ;
#72997=CARTESIAN_POINT ( 'NONE',  ( -89.52287095715011844, -24.33832256527049154, 0.1851278514138623987 ) ) ;
#72998=ORIENTED_EDGE ( 'NONE', *, *, #54445, .F. ) ;
#73000=CARTESIAN_POINT ( 'NONE',  ( -62.62287095715004881, -23.48783264082478794, -1.443836473390068820 ) ) ;
#73003=CARTESIAN_POINT ( 'NONE',  ( -63.58953762381673869, -23.47596703998600276, 11.44779298504227505 ) ) ;
#73004=VERTEX_POINT ( 'NONE', #43261 ) ;
#73005=DIRECTION ( 'NONE',  ( -3.773278334453079030E-23, 0.9999999999976377785, 2.173523156925979128E-06 ) ) ;
#73006=B_SPLINE_CURVE_WITH_KNOTS ( 'NONE', 3,
 ( #45813, #39189, #38185, #54428 ),
 .UNSPECIFIED., .F., .F.,
 ( 4, 4 ),
 ( 0.000000000000000000, 9.999999999994735322E-05 ),
 .UNSPECIFIED. ) ;
#73007=B_SPLINE_CURVE_WITH_KNOTS ( 'NONE', 3,
 ( #93553, #62132, #56527, #47402, #85956, #16433, #86954, #17948 ),
 .UNSPECIFIED., .F., .F.,
 ( 4, 2, 2, 4 ),
 ( 0.000000000000000000, 0.002001079623178227129, 0.003001619434767338959, 0.004002159246356450789 ),
 .UNSPECIFIED. ) ;
#73008=CARTESIAN_POINT ( 'NONE',  ( -17.45619364963476627, 14.87644265977633573, 11.49999999999999645 ) ) ;
#73009=CARTESIAN_POINT ( 'NONE',  ( -12.51292883401962541, 18.98408452820241266, 11.49999999999998934 ) ) ;
#73010=CARTESIAN_POINT ( 'NONE',  ( -71.44728056806559380, -25.14542524405617385, 7.034487670647322055 ) ) ;
#73012=CARTESIAN_POINT ( 'NONE',  ( -90.51172207313412343, -24.15503026093913164, -0.2815557561904542538 ) ) ;
#73015=AXIS2_PLACEMENT_3D ( 'NONE', #94503, #64086, #72678 ) ;
#73016=CARTESIAN_POINT ( 'NONE',  ( 3.414333255021221092, 21.62243999391013105, 11.49999999999998934 ) ) ;
#73019=CARTESIAN_POINT ( 'NONE',  ( -26.49532332504551135, -24.82382521439767942, 2.996894461300356305 ) ) ;
#73022=ORIENTED_EDGE ( 'NONE', *, *, #82964, .F. ) ;
#73023=CARTESIAN_POINT ( 'NONE',  ( -18.16121111207539940, 9.348575961806686152, -1.500000000000002220 ) ) ;
#73025=ORIENTED_EDGE ( 'NONE', *, *, #45108, .T. ) ;
#73026=ORIENTED_EDGE ( 'NONE', *, *, #86902, .T. ) ;
#73027=CARTESIAN_POINT ( 'NONE',  ( 22.09143763772896918, 6.410036269187016522, -1.500000000000002220 ) ) ;
#73028=CARTESIAN_POINT ( 'NONE',  ( -39.52287095715006870, -23.47596703998600631, 11.44779298504229281 ) ) ;
#73029=CARTESIAN_POINT ( 'NONE',  ( -17.93149374516376682, -9.230432107326475233, -1.500000000000002220 ) ) ;
#73033=AXIS2_PLACEMENT_3D ( 'NONE', #90419, #59478, #12285 ) ;
#73034=DIRECTION ( 'NONE',  ( -3.773278334453079030E-23, 0.9999999999976377785, 2.173523156925979128E-06 ) ) ;
#73035=DIRECTION ( 'NONE',  ( 3.773278334444166432E-23, -1.000000000000000000, 0.000000000000000000 ) ) ;
#73036=CARTESIAN_POINT ( 'NONE',  ( 20.92345209525186078, -4.499874906010187026, 11.49999999999999645 ) ) ;
#73037=VERTEX_POINT ( 'NONE', #50872 ) ;
#73039=VECTOR ( 'NONE', #85759, 1000.000000000000227 ) ;
#73041=CARTESIAN_POINT ( 'NONE',  ( -9.338385371603758145, -20.21602636099808237, -1.500000000000002220 ) ) ;
#73042=CARTESIAN_POINT ( 'NONE',  ( -9.011640028862021978, 18.61544202926687674, 11.49999999999998934 ) ) ;
#73044=ORIENTED_EDGE ( 'NONE', *, *, #92917, .F. ) ;
#73045=B_SPLINE_CURVE_WITH_KNOTS ( 'NONE', 3,
 ( #85644, #92744, #63333, #23228 ),
 .UNSPECIFIED., .F., .F.,
 ( 4, 4 ),
 ( 0.1305932534456737681, 0.1395996847177894684 ),
 .UNSPECIFIED. ) ;
#73048=B_SPLINE_CURVE_WITH_KNOTS ( 'NONE', 3,
 ( #25156, #2342, #88076, #80956 ),
 .UNSPECIFIED., .F., .F.,
 ( 4, 4 ),
 ( 0.2706932954563583404, 0.2796997267284738742 ),
 .UNSPECIFIED. ) ;
#73050=VERTEX_POINT ( 'NONE', #98014 ) ;
#73052=CARTESIAN_POINT ( 'NONE',  ( 0.8316226063609513108, 20.92010288561657205, -1.500000000000002220 ) ) ;
#73053=EDGE_CURVE ( 'NONE', #9400, #34090, #52562, .T. ) ;
#73054=CARTESIAN_POINT ( 'NONE',  ( -20.07106029494397248, -8.819774368769808248, 11.49999999999999645 ) ) ;
#73055=CARTESIAN_POINT ( 'NONE',  ( -26.35118574718723750, -24.77993572289172874, 6.568084281490178533 ) ) ;
#73056=CARTESIAN_POINT ( 'NONE',  ( 14.32739804834607256, 17.34395043298086847, 11.49999999999998934 ) ) ;
#73057=CARTESIAN_POINT ( 'NONE',  ( 7.003190781191628744, -19.75400906848480176, -1.500000000000002220 ) ) ;
#73061=ORIENTED_EDGE ( 'NONE', *, *, #63335, .T. ) ;
#73062=EDGE_CURVE ( 'NONE', #94697, #92089, #35561, .T. ) ;
#73063=EDGE_LOOP ( 'NONE', ( #24734, #6869, #7715, #75766 ) ) ;
#73065=EDGE_CURVE ( 'NONE', #37215, #35231, #98541, .T. ) ;
#73066=CARTESIAN_POINT ( 'NONE',  ( -44.52287095715006160, -23.48786465467241058, 11.44779295918255180 ) ) ;
#73067=EDGE_LOOP ( 'NONE', ( #78245, #49840, #24903, #19589 ) ) ;
#73068=CARTESIAN_POINT ( 'NONE',  ( 19.99361899508246765, -7.638522130635823082, -1.500000000000002220 ) ) ;
#73071=CARTESIAN_POINT ( 'NONE',  ( -1.999300432013352058, 20.99099883833691749, 11.49999999999998934 ) ) ;
#73072=CARTESIAN_POINT ( 'NONE',  ( -30.62469739314999373, -24.05799227682217634, 10.47557002954947336 ) ) ;
#73074=PLANE ( 'NONE',  #43769 ) ;
#73075=DIRECTION ( 'NONE',  ( -3.773278334453079030E-23, 0.9999999999976377785, 2.173523156925979128E-06 ) ) ;
#73076=CARTESIAN_POINT ( 'NONE',  ( -129.6239067399031342, -23.48786465467242124, 11.44779295918253936 ) ) ;
#73077=CARTESIAN_POINT ( 'NONE',  ( -12.30081598482267680, 18.28176383447183895, -1.500000000000002220 ) ) ;
#73078=ORIENTED_EDGE ( 'NONE', *, *, #70524, .F. ) ;
#73079=CARTESIAN_POINT ( 'NONE',  ( -65.63297214418551562, -24.63419186844610920, 9.035850630976922204 ) ) ;
#73080=EDGE_CURVE ( 'NONE', #15484, #51301, #29535, .T. ) ;
#73081=CARTESIAN_POINT ( 'NONE',  ( -103.6228709571500559, -29.50250786944525672, 11.44777988621623166 ) ) ;
#73083=CARTESIAN_POINT ( 'NONE',  ( -28.41342374310426067, -24.65886721645977531, 1.590605884330587916 ) ) ;
#73084=CARTESIAN_POINT ( 'NONE',  ( -25.53321325151840426, -24.91491875925870048, 4.756813972840990168 ) ) ;
#73085=CARTESIAN_POINT ( 'NONE',  ( -47.52287095715006160, -24.64898659630528854, 1.056161002820821038 ) ) ;
#73086=CARTESIAN_POINT ( 'NONE',  ( 18.61059577090848549, -10.47110149595715711, 11.49999999999998934 ) ) ;
#73087=DIRECTION ( 'NONE',  ( 0.000000000000000000, -0.9999999999976377785, -2.173523156925979975E-06 ) ) ;
#73088=CARTESIAN_POINT ( 'NONE',  ( -91.16175232477891655, -25.26266127311081888, 3.981777872396910389 ) ) ;
#73089=CARTESIAN_POINT ( 'NONE',  ( -64.64156214474047601, -23.96169478059713498, 10.65365249895718058 ) ) ;
#73090=CARTESIAN_POINT ( 'NONE',  ( -68.58953762381672448, -23.48783264082478439, -1.443836473390067265 ) ) ;
#73091=CARTESIAN_POINT ( 'NONE',  ( -4.885077187424587741, 22.05487924249641551, -1.500000000000002220 ) ) ;
#73093=VERTEX_POINT ( 'NONE', #97529 ) ;
#73094=CARTESIAN_POINT ( 'NONE',  ( -75.62287095715004170, -25.00182538069145366, 7.747789668545099317 ) ) ;
#73095=CARTESIAN_POINT ( 'NONE',  ( -99.58953762381673869, -23.47593901973091235, -1.443836447539001089 ) ) ;
#73096=CARTESIAN_POINT ( 'NONE',  ( -3.970774856468506364, -19.35638658347046714, 11.49999999999999645 ) ) ;
#73097=CARTESIAN_POINT ( 'NONE',  ( -45.62287095715004881, -24.99156045073392463, 7.747789690856161648 ) ) ;
#73098=CARTESIAN_POINT ( 'NONE',  ( -67.52209883245490118, -23.48783264082477018, -1.443836473390094799 ) ) ;
#73099=ADVANCED_FACE ( 'NONE', ( #58986 ), #67598, .F. ) ;
#73101=CARTESIAN_POINT ( 'NONE',  ( -117.6228709571500417, -24.65952944569305316, 1.056160979905706121 ) ) ;
#73104=CARTESIAN_POINT ( 'NONE',  ( -21.09935167195790839, -4.734744157926700225, -1.500000000000002220 ) ) ;
#73106=CARTESIAN_POINT ( 'NONE',  ( -19.00951991574052968, 3.723548053296564575, -1.500000000000002220 ) ) ;
#73108=CARTESIAN_POINT ( 'NONE',  ( -81.17551393562025908, -25.07642019275565204, 7.403513165760432280 ) ) ;
#73109=CARTESIAN_POINT ( 'NONE',  ( -7.851535696030730982, 18.15458241006858131, 11.49999999999998934 ) ) ;
#73110=EDGE_CURVE ( 'NONE', #100015, #6511, #86333, .T. ) ;
#73111=VECTOR ( 'NONE', #66250, 1000.000000000000114 ) ;
#73113=CARTESIAN_POINT ( 'NONE',  ( 20.23811035156253979, -1.552196809741442696, 11.49999999999999645 ) ) ;
#73115=EDGE_CURVE ( 'NONE', #13904, #27148, #4035, .T. ) ;
#73117=CARTESIAN_POINT ( 'NONE',  ( -67.52287095715007581, -23.96177878511310055, 10.65340807706329329 ) ) ;
#73120=CARTESIAN_POINT ( 'NONE',  ( -122.6228709571500417, -23.47596703998600631, 11.44779298504227860 ) ) ;
#73123=CARTESIAN_POINT ( 'NONE',  ( -1.415466703587968667, 19.98303252902060834, 11.49999999999998934 ) ) ;
#73125=ORIENTED_EDGE ( 'NONE', *, *, #47645, .T. ) ;
#73126=FACE_OUTER_BOUND ( 'NONE', #87136, .T. ) ;
#73127=PLANE ( 'NONE',  #33194 ) ;
#73128=CARTESIAN_POINT ( 'NONE',  ( -80.29320949403980023, -25.30554951654463736, 4.971011992112520872 ) ) ;
#73129=CARTESIAN_POINT ( 'NONE',  ( -51.62287095715005592, -29.50250786944525672, 11.44777988621624054 ) ) ;
#73130=CARTESIAN_POINT ( 'NONE',  ( -73.59659251472847075, -23.96119346886880663, -0.6495511937832115779 ) ) ;
#73131=EDGE_CURVE ( 'NONE', #16349, #59175, #13777, .T. ) ;
#73133=CARTESIAN_POINT ( 'NONE',  ( -50.02720224525958770, -25.12100811749006724, 7.112893600995336740 ) ) ;
#73135=EDGE_CURVE ( 'NONE', #33464, #49490, #74307, .T. ) ;
#73136=CARTESIAN_POINT ( 'NONE',  ( -17.48930418531667996, -10.34094407820366612, 11.49999999999998934 ) ) ;
#73138=CARTESIAN_POINT ( 'NONE',  ( -3.987988226355533072, 22.59150145119509290, 11.49999999999998934 ) ) ;
#73140=CARTESIAN_POINT ( 'NONE',  ( -127.6238337642146803, -24.35071581493543746, 9.817618358456011052 ) ) ;
#73141=EDGE_CURVE ( 'NONE', #98739, #49798, #89925, .T. ) ;
#73143=CARTESIAN_POINT ( 'NONE',  ( -50.62287095715005592, -29.50249982740957577, 7.747779886224967605 ) ) ;
#73145=CARTESIAN_POINT ( 'NONE',  ( -49.31927893949910668, -25.12215271391963611, 6.419594345602365415 ) ) ;
#73147=CARTESIAN_POINT ( 'NONE',  ( -17.82860346875387947, 11.52481846644873187, 11.49999999999999645 ) ) ;
#73148=CARTESIAN_POINT ( 'NONE',  ( 10.50125231818214289, 19.49540335892314502, -1.500000000000002220 ) ) ;
#73150=CARTESIAN_POINT ( 'NONE',  ( 9.149160795417088821, -18.46424698110740437, -1.500000000000002220 ) ) ;
#73152=CARTESIAN_POINT ( 'NONE',  ( -94.52287095715006160, -23.48786465467242479, 11.44779295918254292 ) ) ;
#73153=VERTEX_POINT ( 'NONE', #45252 ) ;
#73154=CARTESIAN_POINT ( 'NONE',  ( -54.54196740513740593, -24.34968618360932879, 0.1864209137778771175 ) ) ;
#73155=DIRECTION ( 'NONE',  ( -3.773278334453080206E-23, 0.9999999999976377785, 2.173523156925979975E-06 ) ) ;
#73156=VERTEX_POINT ( 'NONE', #39629 ) ;
#73160=CARTESIAN_POINT ( 'NONE',  ( -81.48149462243461016, -25.24685308744633261, 6.293942982122115559 ) ) ;
#73162=CARTESIAN_POINT ( 'NONE',  ( -20.13249939377427111, -5.111880259578561514, -1.500000000000002220 ) ) ;
#73164=CARTESIAN_POINT ( 'NONE',  ( -6.179238894844691465, -20.81818906610659425, 11.49999999999999645 ) ) ;
#73165=ORIENTED_EDGE ( 'NONE', *, *, #9626, .T. ) ;
#73166=CARTESIAN_POINT ( 'NONE',  ( -99.11920994418380815, -25.30018492339840108, 5.369493761298492096 ) ) ;
#73167=CARTESIAN_POINT ( 'NONE',  ( -111.7095396657709756, -25.25156236136107779, 3.853968145065129747 ) ) ;
#73168=CARTESIAN_POINT ( 'NONE',  ( 22.28251467978060063, -2.329348454117679879, 11.49999999999998934 ) ) ;
#73169=DIRECTION ( 'NONE',  ( -3.773278334453079618E-23, 0.9999999999976377785, 2.173523156925979975E-06 ) ) ;
#73171=ORIENTED_EDGE ( 'NONE', *, *, #59050, .T. ) ;
#73173=AXIS2_PLACEMENT_3D ( 'NONE', #16686, #49167, #9078 ) ;
#73176=ORIENTED_EDGE ( 'NONE', *, *, #98386, .F. ) ;
#73178=CARTESIAN_POINT ( 'NONE',  ( -87.62287095715002749, -23.94994826722515668, -0.6494450866351715312 ) ) ;
#73179=EDGE_CURVE ( 'NONE', #17861, #41986, #63360, .T. ) ;
#73180=ORIENTED_EDGE ( 'NONE', *, *, #73946, .F. ) ;
#73181=CARTESIAN_POINT ( 'NONE',  ( -10.79823215447539653, -18.26288818932900071, -1.500000000000002220 ) ) ;
#73183=EDGE_LOOP ( 'NONE', ( #6497, #52802, #35112, #96106, #63723, #2104, #58926, #90881, #8031, #8283, #81118, #56807, #95124, #31910, #92387, #72, #33527, #99226, #29457, #41860, #56208, #11513, #2371, #48358, #69439, #12209, #18640, #379, #56347, #85227, #42869, #9493, #19521, #51306, #38190, #95014, #50551, #91178, #82981, #88265, #48172, #92506, #39582, #56278, #24970, #59544, #48500, #25370, #10362, #45832, #20824, #82773, #57191, #60810, #29688, #2251, #5862, #55806, #72533, #75953, #86364, #13093, #90850, #87110, #31875, #22077, #682, #93134, #77936, #65134, #38623, #95744, #73554, #64336, #7381, #36036, #93345, #28871, #49493, #4005, #33694, #94725, #85132, #71646, #92876, #6010, #77686, #76601, #64984, #61388, #54447, #93350, #29506, #94998, #35115, #85510, #44376, #73906, #58951, #55303, #45347, #21360, #37939, #72129, #5417, #78261, #72292, #30461, #46289, #66426, #43633, #32196, #94158, #47221, #87266, #11091, #62792, #66698, #27839, #26449, #87520, #28630, #75997, #30615, #24478, #57197, #25758, #73727, #86461, #64565, #40736, #91872, #75294, #55936, #39744, #48678, #20519, #88998, #11488, #91608, #66245, #34814, #58182, #44076, #19680, #50319, #29687, #41876, #14615, #55563, #97045, #65780, #21181, #65579, #88768, #85936, #7358, #34868, #91922, #63309, #41436, #6870, #77044, #60339, #19150, #39768, #81160, #15236, #72425, #89589, #66684, #87975, #14345, #12536, #30853, #78507, #100241, #2682, #98556, #62405, #34975, #37840, #3430, #605, #50378, #14782, #13884, #92968, #43687, #26100, #71315, #56716, #33038, #48833, #49075, #43700, #55772, #14514, #136, #77676, #61544, #98906 ) ) ;
#73184=CARTESIAN_POINT ( 'NONE',  ( -88.55825198115908847, -23.73766607897670156, -1.055555164236456678 ) ) ;
#73185=CARTESIAN_POINT ( 'NONE',  ( 12.52028139621776326, 17.89958603277719718, 11.49999999999998934 ) ) ;
#73186=CARTESIAN_POINT ( 'NONE',  ( -103.5600759584140889, -23.48786465467241058, 11.44779295918254292 ) ) ;
#73187=FACE_OUTER_BOUND ( 'NONE', #25411, .T. ) ;
#73189=CARTESIAN_POINT ( 'NONE',  ( -18.37190169643047355, -11.86832528159398237, -1.500000000000002220 ) ) ;
#73191=ORIENTED_EDGE ( 'NONE', *, *, #8472, .F. ) ;
#73193=CARTESIAN_POINT ( 'NONE',  ( -73.52287095715007581, -24.64898659630528854, 1.056161002820824368 ) ) ;
#73195=EDGE_CURVE ( 'NONE', #68291, #96886, #45745, .T. ) ;
#73196=B_SPLINE_CURVE_WITH_KNOTS ( 'NONE', 3,
 ( #33890, #35884, #66854, #95786 ),
 .UNSPECIFIED., .F., .F.,
 ( 4, 4 ),
 ( 0.000000000000000000, 9.999999999999592548E-05 ),
 .UNSPECIFIED. ) ;
#73197=ORIENTED_EDGE ( 'NONE', *, *, #53122, .F. ) ;
#73198=CARTESIAN_POINT ( 'NONE',  ( -30.58903781818379741, -24.99239904628540643, 7.801777447997523041 ) ) ;
#73200=ORIENTED_EDGE ( 'NONE', *, *, #52219, .T. ) ;
#73201=PLANE ( 'NONE',  #40444 ) ;
#73202=CARTESIAN_POINT ( 'NONE',  ( -30.65075255989291492, -23.47618869255534690, -1.443836447538997314 ) ) ;
#73203=CARTESIAN_POINT ( 'NONE',  ( -20.86817740539179056, 4.147639786170328691, 11.49999999999998934 ) ) ;
#73204=DIRECTION ( 'NONE',  ( 0.000000000000000000, 2.173523156925980399E-06, -0.9999999999976378895 ) ) ;
#73205=FACE_OUTER_BOUND ( 'NONE', #74527, .T. ) ;
#73206=CARTESIAN_POINT ( 'NONE',  ( -85.58930583537424752, -24.52300882791530157, 0.6510814631126254914 ) ) ;
#73208=CARTESIAN_POINT ( 'NONE',  ( -18.32239908988104204, -6.426282940459683068, -1.500000000000002220 ) ) ;
#73209=AXIS2_PLACEMENT_3D ( 'NONE', #2308, #74305, #20014 ) ;
#73210=CARTESIAN_POINT ( 'NONE',  ( -117.5170211865436727, -24.51419770103158768, 9.386484678747166299 ) ) ;
#73211=ORIENTED_EDGE ( 'NONE', *, *, #1770, .F. ) ;
#73212=CARTESIAN_POINT ( 'NONE',  ( 16.94836550497923966, -9.742303593519430649, 11.49999999999999645 ) ) ;
#73214=CARTESIAN_POINT ( 'NONE',  ( -29.58500155169703660, -25.10124537647697451, 6.766630343226909261 ) ) ;
#73217=CARTESIAN_POINT ( 'NONE',  ( -32.58953762381672448, -23.48786465467240347, 11.44779295918255535 ) ) ;
#73218=CARTESIAN_POINT ( 'NONE',  ( -80.58953762381673869, -23.47596703998600276, 11.44779298504227683 ) ) ;
#73220=CARTESIAN_POINT ( 'NONE',  ( 16.89532177248590372, -10.13005384644002227, 11.49999999999998934 ) ) ;
#73221=ORIENTED_EDGE ( 'NONE', *, *, #72702, .T. ) ;
#73222=VECTOR ( 'NONE', #21301, 1000.000000000000114 ) ;
#73223=CARTESIAN_POINT ( 'NONE',  ( -94.62287095715004170, -24.33832256527048088, 0.1851278514138620657 ) ) ;
#73225=B_SPLINE_CURVE_WITH_KNOTS ( 'NONE', 3,
 ( #40653, #18310, #64518, #77307 ),
 .UNSPECIFIED., .F., .F.,
 ( 4, 4 ),
 ( 2.775557561562891351E-17, 0.0001000000000000167286 ),
 .UNSPECIFIED. ) ;
#73230=CARTESIAN_POINT ( 'NONE',  ( -47.63367723631196071, -24.34968618360933590, 0.1864209137778879144 ) ) ;
#73231=CARTESIAN_POINT ( 'NONE',  ( -97.55776846943201974, -23.73791477778912196, 11.05961554403170410 ) ) ;
#73232=CARTESIAN_POINT ( 'NONE',  ( -45.62287095715004881, -29.50250786944525672, 11.44777988621624054 ) ) ;
#73233=CARTESIAN_POINT ( 'NONE',  ( -69.34303308397305443, -25.24515236888725056, 6.209207408895393243 ) ) ;
#73235=CARTESIAN_POINT ( 'NONE',  ( -17.52048005523606022, -9.576713672051738513, -1.500000000000002220 ) ) ;
#73236=CARTESIAN_POINT ( 'NONE',  ( -0.07697111846721775563, -22.05354838441670040, 9.879314768251401091 ) ) ;
#73237=CARTESIAN_POINT ( 'NONE',  ( 15.94990109002195489, -11.90149544800030590, -1.500000000000002220 ) ) ;
#73239=CARTESIAN_POINT ( 'NONE',  ( -71.52287095715007581, -24.64898659630528854, 1.056161002820824368 ) ) ;
#73240=VECTOR ( 'NONE', #5462, 1000.000000000000114 ) ;
#73244=CARTESIAN_POINT ( 'NONE',  ( 16.81283763619640936, 12.23492182941471107, 11.49999999999999645 ) ) ;
#73246=CARTESIAN_POINT ( 'NONE',  ( -59.92287095715005307, -23.47593901973090169, -1.443836447538997536 ) ) ;
#73247=CARTESIAN_POINT ( 'NONE',  ( -15.22011711465338912, -17.00649957279452451, 11.49999999999999645 ) ) ;
#73248=VERTEX_POINT ( 'NONE', #84294 ) ;
#73249=ADVANCED_FACE ( 'NONE', ( #54869 ), #32018, .F. ) ;
#73253=CARTESIAN_POINT ( 'NONE',  ( 15.52975653788041122, 12.98207780544785628, -1.500000000000002220 ) ) ;
#73254=DIRECTION ( 'NONE',  ( -1.000000000000000000, -3.773278334444166432E-23, -8.201307841325785021E-29 ) ) ;
#73256=EDGE_CURVE ( 'NONE', #15801, #91381, #83998, .T. ) ;
#73257=ADVANCED_FACE ( 'NONE', ( #30008 ), #100002, .T. ) ;
#73258=CARTESIAN_POINT ( 'NONE',  ( -84.52287095715004739, -24.50216790748206463, 0.6166512839542488411 ) ) ;
#73259=EDGE_CURVE ( 'NONE', #16731, #95088, #566, .T. ) ;
#73260=ORIENTED_EDGE ( 'NONE', *, *, #61577, .T. ) ;
#73261=CARTESIAN_POINT ( 'NONE',  ( -101.9507253916653440, -29.50249654204571215, 6.236241424690079249 ) ) ;
#73262=CARTESIAN_POINT ( 'NONE',  ( -125.6228709571500843, -25.00158670708909625, 2.256160236439166855 ) ) ;
#73263=CARTESIAN_POINT ( 'NONE',  ( 3.179702300980958185, 19.78100630842630281, -1.500000000000002220 ) ) ;
#73264=CARTESIAN_POINT ( 'NONE',  ( -19.58807393344005376, -7.628504261335002923, 11.49999999999999645 ) ) ;
#73267=CARTESIAN_POINT ( 'NONE',  ( -79.52287095715006160, -24.64965694238575011, 8.947790433994198267 ) ) ;
#73268=CARTESIAN_POINT ( 'NONE',  ( 17.21905055353458991, -13.78536315820828229, -1.500000000000002220 ) ) ;
#73269=FACE_OUTER_BOUND ( 'NONE', #17814, .T. ) ;
#73271=DIRECTION ( 'NONE',  ( 0.000000000000000000, -0.9999999999976377785, -2.173523156925979975E-06 ) ) ;
#73273=CARTESIAN_POINT ( 'NONE',  ( -89.81226385320383088, -25.27880950044345454, 5.947789066509452383 ) ) ;
#73274=CARTESIAN_POINT ( 'NONE',  ( -31.65060625173388331, -23.96119346886880663, -0.6495511937832003646 ) ) ;
#73278=CARTESIAN_POINT ( 'NONE',  ( -61.24303308397303880, -25.03284409833926105, 7.563174216509380265 ) ) ;
#73279=CARTESIAN_POINT ( 'NONE',  ( -51.52287095715006870, -24.64898659630367206, 1.056161002820821038 ) ) ;
#73280=CARTESIAN_POINT ( 'NONE',  ( 3.385237411341575964, -20.22741857368478335, -1.500000000000002220 ) ) ;
#73281=EDGE_CURVE ( 'NONE', #6893, #33865, #8873, .T. ) ;
#73282=VERTEX_POINT ( 'NONE', #30512 ) ;
#73283=FACE_OUTER_BOUND ( 'NONE', #41070, .T. ) ;
#73285=CARTESIAN_POINT ( 'NONE',  ( -83.52287095715007581, -24.51283580621365488, 0.6167428607019708187 ) ) ;
#73286=CARTESIAN_POINT ( 'NONE',  ( -18.97848940637192428, 11.77069306843248064, -1.500000000000002220 ) ) ;
#73288=CARTESIAN_POINT ( 'NONE',  ( -124.6228709571500417, -23.96127896941633750, -0.6493128931037770446 ) ) ;
#73292=DIRECTION ( 'NONE',  ( 0.000000000000000000, 0.9999999999976377785, 2.173523156925979128E-06 ) ) ;
#73294=CARTESIAN_POINT ( 'NONE',  ( -20.80165436122882383, -1.723964017131293103, -1.500000000000002220 ) ) ;
#73296=EDGE_LOOP ( 'NONE', ( #72758, #79807, #46089, #80857 ) ) ;
#73297=CARTESIAN_POINT ( 'NONE',  ( -39.38343800729271038, -25.18497175702170665, 3.293004123648116455 ) ) ;
#73299=ORIENTED_EDGE ( 'NONE', *, *, #34657, .F. ) ;
#73300=ORIENTED_EDGE ( 'NONE', *, *, #63293, .F. ) ;
#73301=CARTESIAN_POINT ( 'NONE',  ( -69.62994293422308090, -25.03149333592383385, 7.382559687064914833 ) ) ;
#73302=CARTESIAN_POINT ( 'NONE',  ( -0.5131542516139314669, 21.03015271272555253, -1.500000000000002220 ) ) ;
#73305=LINE ( 'NONE', #74779, #4491 ) ;
#73306=CARTESIAN_POINT ( 'NONE',  ( -120.5196203229499616, -24.15602025860899360, 10.28564288303534902 ) ) ;
#73307=CARTESIAN_POINT ( 'NONE',  ( -28.62287095715004881, -23.31954350884483773, -1.443835782653508426 ) ) ;
#73308=CARTESIAN_POINT ( 'NONE',  ( -49.62091712621314343, -25.14804027490129457, 3.048647684539328662 ) ) ;
#73309=CARTESIAN_POINT ( 'NONE',  ( -17.90551237062050305, -12.20792721910736667, -1.500000000000002220 ) ) ;
#73311=CARTESIAN_POINT ( 'NONE',  ( 22.17158117043571863, -1.905908075979310334, 11.49999999999999645 ) ) ;
#73313=CARTESIAN_POINT ( 'NONE',  ( -51.44586644541745812, -25.31441856498040011, 5.815367604029775705 ) ) ;
#73315=CARTESIAN_POINT ( 'NONE',  ( -101.2228709571500644, -23.47593901973090169, -1.443836447538996870 ) ) ;
#73316=EDGE_CURVE ( 'NONE', #32133, #80860, #51292, .T. ) ;
#73317=ORIENTED_EDGE ( 'NONE', *, *, #59769, .T. ) ;
#73319=CARTESIAN_POINT ( 'NONE',  ( -105.5228709571500758, -23.47596703998600631, 11.44779298504228038 ) ) ;
#73320=EDGE_LOOP ( 'NONE', ( #47946, #14805, #38784, #73770 ) ) ;
#73321=VECTOR ( 'NONE', #13409, 1000.000000000000227 ) ;
#73322=EDGE_LOOP ( 'NONE', ( #22197, #41615, #23873, #28347 ) ) ;
#73324=DIRECTION ( 'NONE',  ( -3.773278334453079030E-23, 0.9999999999976377785, 2.173523156925979128E-06 ) ) ;
#73325=FACE_OUTER_BOUND ( 'NONE', #78233, .T. ) ;
#73326=CARTESIAN_POINT ( 'NONE',  ( -48.62287095715005592, -24.51283580621362646, 0.6167428607019825870 ) ) ;
#73327=CARTESIAN_POINT ( 'NONE',  ( -32.62287095715004881, -24.65952944569304250, 1.056160979905691688 ) ) ;
#73328=ORIENTED_EDGE ( 'NONE', *, *, #4696, .F. ) ;
#73329=CARTESIAN_POINT ( 'NONE',  ( -130.5728709571501156, -23.71408096108764596, -1.258868304936411109 ) ) ;
#73330=CARTESIAN_POINT ( 'NONE',  ( 22.29217321540274099, 2.676729263222305644, -1.500000000000002220 ) ) ;
#73333=FACE_OUTER_BOUND ( 'NONE', #1435, .T. ) ;
#73336=CARTESIAN_POINT ( 'NONE',  ( -125.5228709571501184, -23.85196035787549462, -0.8779234886354203571 ) ) ;
#73337=CARTESIAN_POINT ( 'NONE',  ( -97.24911545764794596, -24.57215472537218659, 9.174899246800713115 ) ) ;
#73338=CARTESIAN_POINT ( 'NONE',  ( -7.889300446747370188, -17.95381117360125955, 11.49999999999998934 ) ) ;
#73339=B_SPLINE_SURFACE_WITH_KNOTS ( 'NONE', 3, 3, ( 
 ( #60, #22373, #53357, #70069 ),
 ( #85290, #54357, #84285, #61473 ),
 ( #8174, #46742, #38112, #21874 ),
 ( #7164, #13767, #99993, #92396 ),
 ( #77166, #44745, #15777, #37619 ),
 ( #23374, #91897, #29499, #83289 ),
 ( #75666, #31003, #7670, #45735 ) ),
 .UNSPECIFIED., .F., .F., .F.,
 ( 4, 3, 4 ),
 ( 4, 4 ),
 ( 0.7945040050992236980, 0.8970133687736496775, 0.9995227324480755460 ),
 ( 0.2295523296736148022, 0.2306710308168615775 ),
 .UNSPECIFIED. ) ;
#73342=CARTESIAN_POINT ( 'NONE',  ( -21.46803524902295024, 1.580295693706654347, 11.49999999999998934 ) ) ;
#73344=CARTESIAN_POINT ( 'NONE',  ( -71.08634551208074015, -25.25639530652865616, 6.775733508723637222 ) ) ;
#73345=CARTESIAN_POINT ( 'NONE',  ( -33.62287095715005592, -29.50248528299804818, 1.056150453629029817 ) ) ;
#73346=CARTESIAN_POINT ( 'NONE',  ( -108.6228709571500701, -23.48783264082478794, -1.443836473390060604 ) ) ;
#73347=CARTESIAN_POINT ( 'NONE',  ( -1.334576548209915225, -22.92891363262047832, -1.500000000000002220 ) ) ;
#73351=PLANE ( 'NONE',  #84717 ) ;
#73352=CARTESIAN_POINT ( 'NONE',  ( 18.81927703376926786, -7.057843677351100631, 11.49999999999999645 ) ) ;
#73354=CARTESIAN_POINT ( 'NONE',  ( -32.63551089020518958, -24.35071581493542681, 9.817618358456035921 ) ) ;
#73356=FACE_OUTER_BOUND ( 'NONE', #81050, .T. ) ;
#73357=CARTESIAN_POINT ( 'NONE',  ( -65.62287095715005592, -23.84047902841601640, -0.8780736468305807563 ) ) ;
#73359=CARTESIAN_POINT ( 'NONE',  ( -9.893332137849947472, -17.22304987741864579, 11.49999999999998934 ) ) ;
#73360=CARTESIAN_POINT ( 'NONE',  ( -57.62287095715004881, -29.50248528299804818, 1.056150453629034924 ) ) ;
#73361=CARTESIAN_POINT ( 'NONE',  ( -14.12090166725071327, 13.77431136191591143, -1.500000000000002220 ) ) ;
#73368=CARTESIAN_POINT ( 'NONE',  ( 19.39738937107077632, -6.937168198526852514, 11.49999999999999645 ) ) ;
#73370=CARTESIAN_POINT ( 'NONE',  ( -14.08738070862771963, 17.71811851510361535, 11.49999999999999645 ) ) ;
#73372=CARTESIAN_POINT ( 'NONE',  ( -69.50411869601543913, -25.12219058395973903, 6.704350939376936047 ) ) ;
#73373=CARTESIAN_POINT ( 'NONE',  ( -50.38822539166535108, -25.31267346029541088, 4.736250531364077254 ) ) ;
#73375=ADVANCED_FACE ( 'NONE', ( #62992 ), #34028, .T. ) ;
#73376=CARTESIAN_POINT ( 'NONE',  ( -26.85174826923451974, -24.61460070623850882, 8.053060507491462516 ) ) ;
#73377=EDGE_CURVE ( 'NONE', #68707, #40883, #7609, .T. ) ;
#73378=DIRECTION ( 'NONE',  ( 0.000000000000000000, -0.9999999999976377785, -2.173523156925979552E-06 ) ) ;
#73379=EDGE_CURVE ( 'NONE', #93213, #35233, #10137, .T. ) ;
#73381=B_SPLINE_CURVE_WITH_KNOTS ( 'NONE', 3,
 ( #22628, #59224, #43991, #68331, #91653, #53617, #74923, #21141, #29764, #60730, #22132, #6922, #45996, #5924 ),
 .UNSPECIFIED., .F., .F.,
 ( 4, 2, 2, 2, 2, 2, 4 ),
 ( 0.000000000000000000, 0.0002566272901473193595, 0.0005132545802946387190, 0.001026509160589279390, 0.001539763740883919735, 0.001796391031031241209, 0.002053018321178562682 ),
 .UNSPECIFIED. ) ;
#73382=ORIENTED_EDGE ( 'NONE', *, *, #13099, .T. ) ;
#73384=CARTESIAN_POINT ( 'NONE',  ( -98.52287095715006160, -23.47596703998600631, 11.44779298504228215 ) ) ;
#73385=CARTESIAN_POINT ( 'NONE',  ( -22.87863416751641310, 0.2071024363326711970, 11.49999999999998934 ) ) ;
#73386=CARTESIAN_POINT ( 'NONE',  ( -105.5895376238167245, -24.99132157543166954, 2.256160258750668390 ) ) ;
#73387=CARTESIAN_POINT ( 'NONE',  ( -113.6281207077734479, -23.96169478059713853, 10.65365249895717348 ) ) ;
#73388=CARTESIAN_POINT ( 'NONE',  ( -32.52287095715006160, -23.48783264083359867, -1.443836473376375329 ) ) ;
#73389=DIRECTION ( 'NONE',  ( -3.773278334453079618E-23, 0.9999999999976377785, 2.173523156925979975E-06 ) ) ;
#73390=CARTESIAN_POINT ( 'NONE',  ( -10.06026007034034464, -20.14757889648583244, 11.49999999999999645 ) ) ;
#73391=VERTEX_POINT ( 'NONE', #87304 ) ;
#73392=CARTESIAN_POINT ( 'NONE',  ( -89.81226385320383088, -25.23397913219354649, 6.409327625488847602 ) ) ;
#73393=CARTESIAN_POINT ( 'NONE',  ( 20.57779966680088890, -7.652443150423321683, -1.500000000000002220 ) ) ;
#73394=CARTESIAN_POINT ( 'NONE',  ( -44.52203580682488848, -23.48786465467240347, 11.44779295918255357 ) ) ;
#73395=CARTESIAN_POINT ( 'NONE',  ( -29.14051086615235420, -25.21724692324598394, 6.215525031367211461 ) ) ;
#73398=CARTESIAN_POINT ( 'NONE',  ( -63.62287095715007723, -23.47596703998600631, 11.44779298504227683 ) ) ;
#73399=CARTESIAN_POINT ( 'NONE',  ( -111.6228709571500275, -24.33832256526968862, 0.1851278514119932828 ) ) ;
#73401=CARTESIAN_POINT ( 'NONE',  ( -29.52287095715006870, -23.40099448348795264, -1.443836171194820883 ) ) ;
#73402=CARTESIAN_POINT ( 'NONE',  ( -17.91610926057384034, -10.00117247862695358, 11.49999999999998934 ) ) ;
#73403=ORIENTED_EDGE ( 'NONE', *, *, #37008, .F. ) ;
#73406=ORIENTED_EDGE ( 'NONE', *, *, #77253, .T. ) ;
#73407=CARTESIAN_POINT ( 'NONE',  ( -126.5228709571500332, -24.50216790748206108, 0.6166512839542589441 ) ) ;
#73408=CARTESIAN_POINT ( 'NONE',  ( 14.65057173600216345, 17.85730367728733725, 11.49999999999998934 ) ) ;
#73409=CARTESIAN_POINT ( 'NONE',  ( -104.6328494754281877, -23.73791477778912196, 11.05961554403170410 ) ) ;
#73410=CARTESIAN_POINT ( 'NONE',  ( -17.41452279269062586, 10.58001483151439004, -1.500000000000002220 ) ) ;
#73411=ORIENTED_EDGE ( 'NONE', *, *, #50244, .F. ) ;
#73413=CARTESIAN_POINT ( 'NONE',  ( -88.62287095714999907, -23.96127896941631619, -0.6493128931037803753 ) ) ;
#73415=CARTESIAN_POINT ( 'NONE',  ( -57.55620429048338593, -23.48783264082478439, -1.443836473390068376 ) ) ;
#73418=CARTESIAN_POINT ( 'NONE',  ( -61.64687923781919210, -25.21083105912962452, 3.409327675794633361 ) ) ;
#73419=ORIENTED_EDGE ( 'NONE', *, *, #52435, .F. ) ;
#73420=CARTESIAN_POINT ( 'NONE',  ( 5.906898857431191807, -19.90033995357616092, -1.500000000000002220 ) ) ;
#73421=ORIENTED_EDGE ( 'NONE', *, *, #8996, .F. ) ;
#73422=CARTESIAN_POINT ( 'NONE',  ( -101.5221917989304359, -23.48783264082477373, -1.443836473390089248 ) ) ;
#73423=ORIENTED_EDGE ( 'NONE', *, *, #34254, .T. ) ;
#73424=B_SPLINE_SURFACE_WITH_KNOTS ( 'NONE', 3, 3, ( 
 ( #21551, #53532, #83457, #7326 ),
 ( #84456, #13945, #79341, #64152 ),
 ( #7832, #9835, #23540, #38782 ),
 ( #16437, #39775, #9328, #25053 ),
 ( #40788, #24553, #54518, #77827 ),
 ( #85450, #8837, #86459, #8334 ),
 ( #69743, #85961, #39280, #47405 ) ),
 .UNSPECIFIED., .F., .F., .F.,
 ( 4, 3, 4 ),
 ( 4, 4 ),
 ( 0.0004766839783824127277, 0.1029713700210899280, 0.2054660560637974476 ),
 ( 0.2395549359311070492, 0.2406781906944148730 ),
 .UNSPECIFIED. ) ;
#73425=B_SPLINE_CURVE_WITH_KNOTS ( 'NONE', 3,
 ( #46234, #29998, #76166, #6665 ),
 .UNSPECIFIED., .F., .F.,
 ( 4, 4 ),
 ( 0.7810577342095665898, 0.7900641654816820125 ),
 .UNSPECIFIED. ) ;
#73428=ORIENTED_EDGE ( 'NONE', *, *, #64519, .T. ) ;
#73430=DIRECTION ( 'NONE',  ( -3.773278334453080206E-23, 0.9999999999976377785, 2.173523156925979552E-06 ) ) ;
#73432=CARTESIAN_POINT ( 'NONE',  ( -70.65140973383547873, -25.24515049886350582, 5.348842177717589408 ) ) ;
#73433=CARTESIAN_POINT ( 'NONE',  ( -17.89045161427552699, -12.92718102017995641, 11.49999999999999645 ) ) ;
#73434=ORIENTED_EDGE ( 'NONE', *, *, #78181, .F. ) ;
#73435=CARTESIAN_POINT ( 'NONE',  ( -103.5172116781898382, -23.96119346886881019, -0.6495511937832079141 ) ) ;
#73437=CARTESIAN_POINT ( 'NONE',  ( -21.91535228782390732, -5.629186751109307885, -1.500000000000002220 ) ) ;
#73438=ADVANCED_FACE ( 'NONE', ( #80199 ), #71093, .T. ) ;
#73439=CARTESIAN_POINT ( 'NONE',  ( -99.19451705248940243, -25.30269465406787788, 5.270746443602242870 ) ) ;
#73440=ORIENTED_EDGE ( 'NONE', *, *, #61618, .F. ) ;
#73441=VECTOR ( 'NONE', #55523, 1000.000000000000114 ) ;
#73442=VERTEX_POINT ( 'NONE', #32522 ) ;
#73443=CARTESIAN_POINT ( 'NONE',  ( -88.52287095715009002, -23.73934037231757088, 11.05740245334328442 ) ) ;
#73444=EDGE_CURVE ( 'NONE', #63576, #75985, #82730, .T. ) ;
#73445=CARTESIAN_POINT ( 'NONE',  ( -86.55620429048336462, -23.48783264082478084, -1.443836473390063269 ) ) ;
#73446=VERTEX_POINT ( 'NONE', #73097 ) ;
#73447=CARTESIAN_POINT ( 'NONE',  ( -7.741094375770895653, -19.69850519626218599, -1.500000000000002220 ) ) ;
#73449=CARTESIAN_POINT ( 'NONE',  ( -41.58505200082024089, -25.30574842329748719, 5.038258840064731459 ) ) ;
#73450=CARTESIAN_POINT ( 'NONE',  ( 6.212073114426278408, 21.40951068830820958, -1.500000000000002220 ) ) ;
#73451=CARTESIAN_POINT ( 'NONE',  ( -50.34609605362255280, -25.03220906408855484, 7.561522611969397900 ) ) ;
#73452=ORIENTED_EDGE ( 'NONE', *, *, #70732, .F. ) ;
#73453=CARTESIAN_POINT ( 'NONE',  ( -112.5228709571500758, -23.73907113217711284, -1.053371485780540739 ) ) ;
#73458=CARTESIAN_POINT ( 'NONE',  ( -6.230579426152004885, -18.48807627814308674, 11.49999999999998934 ) ) ;
#73459=CARTESIAN_POINT ( 'NONE',  ( 17.68986881342592454, -12.14045624799103962, 11.49999999999998934 ) ) ;
#73461=DIRECTION ( 'NONE',  ( 0.000000000000000000, 0.9999999999976377785, 2.173523156925979128E-06 ) ) ;
#73462=FACE_OUTER_BOUND ( 'NONE', #26460, .T. ) ;
#73463=CARTESIAN_POINT ( 'NONE',  ( -16.48365427610503886, -15.78576583860491489, -1.500000000000002220 ) ) ;
#73465=CARTESIAN_POINT ( 'NONE',  ( -102.5550617024446183, -23.96119346886881729, -0.6495511937831880411 ) ) ;
#73466=LINE ( 'NONE', #13045, #60578 ) ;
#73467=CARTESIAN_POINT ( 'NONE',  ( 7.348632388941331861, 18.53259892055224611, 11.49999999999999645 ) ) ;
#73468=CARTESIAN_POINT ( 'NONE',  ( -101.6228709571500275, -23.73934037231757799, 11.05740245334328087 ) ) ;
#73469=AXIS2_PLACEMENT_3D ( 'NONE', #25903, #74084, #12165 ) ;
#73470=CARTESIAN_POINT ( 'NONE',  ( -39.48564304424269977, -24.51419770103158413, 9.386484678747189392 ) ) ;
#73471=CARTESIAN_POINT ( 'NONE',  ( -48.52204688060093929, -23.48783264082477729, -1.443836473390069264 ) ) ;
#73474=CARTESIAN_POINT ( 'NONE',  ( -33.01384891882022288, -24.87219037988794312, 1.747789950295619787 ) ) ;
#73475=CARTESIAN_POINT ( 'NONE',  ( 16.47784684176308545, -14.13017478139203220, 11.49999999999998934 ) ) ;
#73476=CARTESIAN_POINT ( 'NONE',  ( -50.60270360225540998, -25.04428781446249275, 7.557560453701762881 ) ) ;
#73477=CARTESIAN_POINT ( 'NONE',  ( -10.41718274906430786, -16.55731393670301088, -1.500000000000002220 ) ) ;
#73478=CARTESIAN_POINT ( 'NONE',  ( -55.59972936617020878, -24.15602025860896518, 10.28564288303535257 ) ) ;
#73479=DIRECTION ( 'NONE',  ( 3.773278334444167608E-23, -1.000000000000000000, 0.000000000000000000 ) ) ;
#73480=CARTESIAN_POINT ( 'NONE',  ( -18.82070947631147106, 8.064391923812276985, 11.49999999999999645 ) ) ;
#73483=VERTEX_POINT ( 'NONE', #3587 ) ;
#73485=CARTESIAN_POINT ( 'NONE',  ( -69.52287095715006160, -29.50248528299804818, 1.056150453629036701 ) ) ;
#73486=CARTESIAN_POINT ( 'NONE',  ( -45.57257061460039438, -23.48786465467240347, 11.44779295918255002 ) ) ;
#73488=CARTESIAN_POINT ( 'NONE',  ( -109.5537054002563622, -24.15543982623907482, -0.2315651400026587370 ) ) ;
#73489=VECTOR ( 'NONE', #67088, 1000.000000000000114 ) ;
#73492=FACE_OUTER_BOUND ( 'NONE', #75507, .T. ) ;
#73494=CARTESIAN_POINT ( 'NONE',  ( 22.51966570110743149, 4.691836548664650053, 11.49999999999999645 ) ) ;
#73495=CARTESIAN_POINT ( 'NONE',  ( 0.6941480231959694658, 22.73124288027050710, 11.49999999999998934 ) ) ;
#73497=B_SPLINE_CURVE_WITH_KNOTS ( 'NONE', 3,
 ( #72157, #77730, #31574, #33584 ),
 .UNSPECIFIED., .F., .F.,
 ( 4, 4 ),
 ( 0.000000000000000000, 1.000000000000000000 ),
 .UNSPECIFIED. ) ;
#73501=CARTESIAN_POINT ( 'NONE',  ( -97.62287095715005592, -23.47593901973091235, -1.443836447539001089 ) ) ;
#73502=CARTESIAN_POINT ( 'NONE',  ( -54.52287095715006870, -24.65952944569304606, 1.056160979905693686 ) ) ;
#73503=ADVANCED_FACE ( 'NONE', ( #43143 ), #66989, .F. ) ;
#73504=CARTESIAN_POINT ( 'NONE',  ( -70.07703791455010389, -25.13739033695690850, 7.077244113302262996 ) ) ;
#73505=CARTESIAN_POINT ( 'NONE',  ( -12.54888962926113827, 17.92887824059606672, -1.500000000000002220 ) ) ;
#73507=B_SPLINE_CURVE_WITH_KNOTS ( 'NONE', 3,
 ( #95715, #73386, #65790, #65297 ),
 .UNSPECIFIED., .F., .F.,
 ( 4, 4 ),
 ( 0.000000000000000000, 9.999999999997510880E-05 ),
 .UNSPECIFIED. ) ;
#73511=ORIENTED_EDGE ( 'NONE', *, *, #47191, .F. ) ;
#73512=CARTESIAN_POINT ( 'NONE',  ( 0.5039804632396667206, -20.40334623801319580, 11.49999999999998934 ) ) ;
#73513=ORIENTED_EDGE ( 'NONE', *, *, #26054, .T. ) ;
#73515=ORIENTED_EDGE ( 'NONE', *, *, #77141, .T. ) ;
#73516=B_SPLINE_CURVE_WITH_KNOTS ( 'NONE', 3,
 ( #56918, #42690, #12207, #89350 ),
 .UNSPECIFIED., .F., .F.,
 ( 4, 4 ),
 ( 2.202873842868165974E-11, 0.001051771062785959547 ),
 .UNSPECIFIED. ) ;
#73517=VERTEX_POINT ( 'NONE', #75064 ) ;
#73518=EDGE_CURVE ( 'NONE', #78484, #36722, #41604, .T. ) ;
#73519=CARTESIAN_POINT ( 'NONE',  ( -9.967090755842360039, -20.75144515299163217, 11.49999999999998934 ) ) ;
#73520=LINE ( 'NONE', #4010, #63263 ) ;
#73521=CARTESIAN_POINT ( 'NONE',  ( 0.4983251850863967269, 20.17815531296474418, -1.500000000000002220 ) ) ;
#73522=ORIENTED_EDGE ( 'NONE', *, *, #50403, .F. ) ;
#73523=DIRECTION ( 'NONE',  ( -3.773278334453079030E-23, 0.9999999999976377785, 2.173523156925979128E-06 ) ) ;
#73526=CARTESIAN_POINT ( 'NONE',  ( -53.51455889064216365, -23.73791477778911840, 11.05961554403170766 ) ) ;
#73527=CARTESIAN_POINT ( 'NONE',  ( -15.71168838272081558, 14.50144224353281786, 11.49999999999999645 ) ) ;
#73528=EDGE_LOOP ( 'NONE', ( #39833, #60232, #73191, #13595 ) ) ;
#73530=ORIENTED_EDGE ( 'NONE', *, *, #53059, .F. ) ;
#73531=CARTESIAN_POINT ( 'NONE',  ( -13.70410651198969809, -17.55484038775568933, 11.49999999999998934 ) ) ;
#73532=CARTESIAN_POINT ( 'NONE',  ( 4.906390264955167169, 20.09725327650800608, 11.49999999999998934 ) ) ;
#73541=CARTESIAN_POINT ( 'NONE',  ( -12.80012119340476140, -16.60591428456014640, -1.500000000000002220 ) ) ;
#73542=CARTESIAN_POINT ( 'NONE',  ( -17.33335002049248530, 13.43749923854009509, 11.49999999999999645 ) ) ;
#73544=CARTESIAN_POINT ( 'NONE',  ( -73.54977362450368616, -24.15620529776628089, 10.23563542870660470 ) ) ;
#73545=CARTESIAN_POINT ( 'NONE',  ( -10.06026007034034464, -20.14757889648583244, 11.49999999999998934 ) ) ;
#73546=CARTESIAN_POINT ( 'NONE',  ( 2.313481123293766206, -20.83243486019555135, 11.49999999999998934 ) ) ;
#73547=CARTESIAN_POINT ( 'NONE',  ( -26.18848782724420232, -24.97067017990783455, 5.990951028626401609 ) ) ;
#73550=FACE_OUTER_BOUND ( 'NONE', #75679, .T. ) ;
#73551=CARTESIAN_POINT ( 'NONE',  ( -68.55620429048340725, -23.47593901973091235, -1.443836447539006196 ) ) ;
#73553=ORIENTED_EDGE ( 'NONE', *, *, #39782, .T. ) ;
#73554=ORIENTED_EDGE ( 'NONE', *, *, #8433, .F. ) ;
#73555=B_SPLINE_CURVE_WITH_KNOTS ( 'NONE', 3,
 ( #16081, #91700, #23187, #54173 ),
 .UNSPECIFIED., .F., .F.,
 ( 4, 4 ),
 ( 0.3300215848131905494, 0.3390280160853059721 ),
 .UNSPECIFIED. ) ;
#73556=CARTESIAN_POINT ( 'NONE',  ( -44.52287095715007581, -23.73934037231757088, 11.05740245334329330 ) ) ;
#73557=VERTEX_POINT ( 'NONE', #96922 ) ;
#73558=CARTESIAN_POINT ( 'NONE',  ( 17.37860173834871347, 12.56526366372364301, -1.500000000000002220 ) ) ;
#73559=EDGE_CURVE ( 'NONE', #33217, #25851, #74091, .T. ) ;
#73560=CARTESIAN_POINT ( 'NONE',  ( -26.09764047488493333, -24.96011088229958830, 5.074688329380741436 ) ) ;
#73561=ORIENTED_EDGE ( 'NONE', *, *, #61400, .T. ) ;
#73562=CARTESIAN_POINT ( 'NONE',  ( 20.91448408463407205, 2.778442817847782020, -1.500000000000002220 ) ) ;
#73563=CARTESIAN_POINT ( 'NONE',  ( -63.52287095715006160, -24.65952944569304606, 1.056160979905695463 ) ) ;
#73566=CARTESIAN_POINT ( 'NONE',  ( -101.5888365374433278, -24.34968618360934300, 0.1864209137778871650 ) ) ;
#73567=CARTESIAN_POINT ( 'NONE',  ( -129.5896345871542508, -24.51419770103158058, 9.386484678747178734 ) ) ;
#73568=CARTESIAN_POINT ( 'NONE',  ( 10.71795340210964120, -19.33932934982082585, -1.500000000000002220 ) ) ;
#73569=ORIENTED_EDGE ( 'NONE', *, *, #62733, .T. ) ;
#73573=CARTESIAN_POINT ( 'NONE',  ( -48.52287095715006160, -23.48786465467241769, 11.44779295918255002 ) ) ;
#73574=CARTESIAN_POINT ( 'NONE',  ( -41.02425807142757463, -25.31624721201647432, 5.449276950507639938 ) ) ;
#73575=CARTESIAN_POINT ( 'NONE',  ( -62.58330144089487135, -24.51419770103156281, 9.386484678747184063 ) ) ;
#73578=CARTESIAN_POINT ( 'NONE',  ( -11.21157863559261791, -18.18922556752850994, 11.49999999999998934 ) ) ;
#73579=CARTESIAN_POINT ( 'NONE',  ( -69.11883240928005989, -25.16874515868137863, 6.888629470625632578 ) ) ;
#73580=CARTESIAN_POINT ( 'NONE',  ( -49.88568991126719254, -25.30060005375480969, 6.009289253917325269 ) ) ;
#73581=CARTESIAN_POINT ( 'NONE',  ( -64.50490266001314410, -24.15620529776628445, 10.23563542870660115 ) ) ;
#73582=PLANE ( 'NONE',  #73469 ) ;
#73584=CARTESIAN_POINT ( 'NONE',  ( 19.88857169258762170, 10.62688394266798930, -1.500000000000002220 ) ) ;
#73585=DIRECTION ( 'NONE',  ( -3.773278334453079618E-23, 0.9999999999976377785, 2.173523156925979975E-06 ) ) ;
#73586=EDGE_LOOP ( 'NONE', ( #72930, #80177, #45835, #63945 ) ) ;
#73587=CARTESIAN_POINT ( 'NONE',  ( -50.44907891876609796, -25.31399901078718884, 5.199047781166664883 ) ) ;
#73588=CARTESIAN_POINT ( 'NONE',  ( -47.62287095715004881, -24.64965695001467694, 8.947790433994185832 ) ) ;
#73589=CARTESIAN_POINT ( 'NONE',  ( -14.27994306655487300, -13.59162091658854798, 11.49999999999999645 ) ) ;
#73590=CARTESIAN_POINT ( 'NONE',  ( -59.62287095715008434, -24.34917612406837861, 0.1852690917426605965 ) ) ;
#73591=CARTESIAN_POINT ( 'NONE',  ( -67.59255334188506481, -24.15543982623906771, -0.2315651400026651485 ) ) ;
#73594=CARTESIAN_POINT ( 'NONE',  ( -29.54861811807234417, -24.60094191855587553, 3.015636009103882298 ) ) ;
#73595=CARTESIAN_POINT ( 'NONE',  ( -75.52287095715007581, -23.48786465467241769, 11.44779295918254469 ) ) ;
#73596=CARTESIAN_POINT ( 'NONE',  ( -4.285004571687458963, -21.18589511591401831, 11.49999999999998934 ) ) ;
#73597=DIRECTION ( 'NONE',  ( 0.000000000000000000, 2.173523156925980399E-06, -0.9999999999976378895 ) ) ;
#73598=CARTESIAN_POINT ( 'NONE',  ( 3.017506814366913481, 19.14668354085002733, -1.500000000000002220 ) ) ;
#73600=B_SPLINE_CURVE_WITH_KNOTS ( 'NONE', 3,
 ( #36164, #60012, #67128, #52886, #22407, #83825 ),
 .UNSPECIFIED., .F., .F.,
 ( 4, 2, 4 ),
 ( 0.000000000000000000, 0.001380901958385393315, 0.002761803916770786630 ),
 .UNSPECIFIED. ) ;
#73601=CARTESIAN_POINT ( 'NONE',  ( -73.52287095715007581, -23.47596703998600631, 11.44779298504228748 ) ) ;
#73602=CARTESIAN_POINT ( 'NONE',  ( 10.99584971316270732, 16.45119811332560289, 11.49999999999998934 ) ) ;
#73604=CARTESIAN_POINT ( 'NONE',  ( 18.19722386731275066, -8.884848157732822216, 11.49999999999999645 ) ) ;
#73606=B_SPLINE_CURVE_WITH_KNOTS ( 'NONE', 3,
 ( #88419, #66604, #88919, #97516, #19390, #18891 ),
 .UNSPECIFIED., .F., .F.,
 ( 4, 2, 4 ),
 ( 0.000000000000000000, 0.001380901958385383774, 0.002761803916770767548 ),
 .UNSPECIFIED. ) ;
#73607=ORIENTED_EDGE ( 'NONE', *, *, #40634, .T. ) ;
#73608=B_SPLINE_SURFACE_WITH_KNOTS ( 'NONE', 3, 3, ( 
 ( #38423, #30812, #61281, #92204 ),
 ( #16575, #22679, #15577, #100294 ),
 ( #61777, #92696, #77469, #7969 ),
 ( #38922, #866, #85591, #69876 ),
 ( #62276, #359, #31307, #31819 ),
 ( #62788, #86097, #78472, #42447 ),
 ( #49554, #57664, #9474, #18089 ) ),
 .UNSPECIFIED., .F., .F., .F.,
 ( 4, 3, 4 ),
 ( 4, 4 ),
 ( 0.0004766839783815382645, 0.1029713700210893729, 0.2054660560637971978 ),
 ( 0.5596363591768273027, 0.5609072989206914661 ),
 .UNSPECIFIED. ) ;
#73610=DIRECTION ( 'NONE',  ( -3.773278334453080206E-23, 0.9999999999976377785, 2.173523156925979975E-06 ) ) ;
#73611=CARTESIAN_POINT ( 'NONE',  ( -75.55620429048340725, -23.48783264082478794, -1.443836473390065489 ) ) ;
#73612=CARTESIAN_POINT ( 'NONE',  ( -62.62287095715004881, -23.48786465467241058, 11.44779295918254824 ) ) ;
#73613=CARTESIAN_POINT ( 'NONE',  ( -58.58953762381673158, -24.64898659630367916, 1.056161002820381611 ) ) ;
#73614=CARTESIAN_POINT ( 'NONE',  ( 15.05167116458888010, 13.23127732593390959, 11.49999999999998934 ) ) ;
#73619=EDGE_CURVE ( 'NONE', #64351, #94960, #47710, .T. ) ;
#73621=CARTESIAN_POINT ( 'NONE',  ( -100.5895376238167245, -24.99156044556203327, 7.747789690856173195 ) ) ;
#73623=DIRECTION ( 'NONE',  ( 0.000000000000000000, 0.9999999999976377785, 2.173523156925979128E-06 ) ) ;
#73624=CARTESIAN_POINT ( 'NONE',  ( -73.63047822457768632, -24.34968618360933590, 0.1864209137778805869 ) ) ;
#73627=CARTESIAN_POINT ( 'NONE',  ( -93.58953762381671027, -24.64898659630367916, 1.056161002820387829 ) ) ;
#73629=CARTESIAN_POINT ( 'NONE',  ( -8.236308187080631171, 18.58821751820538637, 11.49999999999998934 ) ) ;
#73630=ORIENTED_EDGE ( 'NONE', *, *, #11007, .F. ) ;
#73632=CARTESIAN_POINT ( 'NONE',  ( -9.675568039816649701, -20.77828039667204862, 11.49999999999998934 ) ) ;
#73633=CARTESIAN_POINT ( 'NONE',  ( -32.65033202046554806, -23.96119346886880663, -0.6495511937831992544 ) ) ;
#73634=AXIS2_PLACEMENT_3D ( 'NONE', #39455, #95240, #1898 ) ;
#73639=CARTESIAN_POINT ( 'NONE',  ( -18.66175431467001999, 10.11895122522205526, 11.49999999999999645 ) ) ;
#73640=CARTESIAN_POINT ( 'NONE',  ( -20.56814720681451902, 8.302189128749821734, 11.49999999999998934 ) ) ;
#73641=B_SPLINE_CURVE_WITH_KNOTS ( 'NONE', 3,
 ( #98022, #74210, #13287, #37136 ),
 .UNSPECIFIED., .F., .F.,
 ( 4, 4 ),
 ( 0.6709791297726001025, 0.6799855610447156362 ),
 .UNSPECIFIED. ) ;
#73642=CARTESIAN_POINT ( 'NONE',  ( 1.511266892140219920, 20.53031905857337591, 11.49999999999998934 ) ) ;
#73644=CARTESIAN_POINT ( 'NONE',  ( -41.61684277447768920, -23.48783264082477729, -1.443836473390075925 ) ) ;
#73645=ORIENTED_EDGE ( 'NONE', *, *, #41534, .T. ) ;
#73646=CARTESIAN_POINT ( 'NONE',  ( -54.56007898073282547, -23.73766607897669800, -1.055555164236461785 ) ) ;
#73648=EDGE_LOOP ( 'NONE', ( #21660, #85261, #28366, #95418 ) ) ;
#73649=ORIENTED_EDGE ( 'NONE', *, *, #96289, .F. ) ;
#73650=VERTEX_POINT ( 'NONE', #81700 ) ;
#73651=DIRECTION ( 'NONE',  ( 0.8368789961609479633, -1.189760341428526303E-06, 0.5473879298844910313 ) ) ;
#73652=CARTESIAN_POINT ( 'NONE',  ( -28.57383146581955202, -24.50354187648331816, 8.947790409070465856 ) ) ;
#73654=CARTESIAN_POINT ( 'NONE',  ( -9.565632364391108311, -18.43008791299702764, -1.500000000000002220 ) ) ;
#73655=CARTESIAN_POINT ( 'NONE',  ( 20.36105213711617878, 7.643125777291208678, 11.49999999999999645 ) ) ;
#73657=CARTESIAN_POINT ( 'NONE',  ( -113.6228709571500701, -23.73934037231757799, 11.05740245334328264 ) ) ;
#73658=CARTESIAN_POINT ( 'NONE',  ( -28.52287095715005805, -23.32378116302990279, 11.44779301262222049 ) ) ;
#73659=CARTESIAN_POINT ( 'NONE',  ( -21.98280116189361877, -4.439423430357301470, 11.49999999999998934 ) ) ;
#73664=CARTESIAN_POINT ( 'NONE',  ( -98.52287095715007581, -23.72773821059536914, 11.05748984161097503 ) ) ;
#73665=LINE ( 'NONE', #35611, #74999 ) ;
#73666=AXIS2_PLACEMENT_3D ( 'NONE', #74944, #83563, #75947 ) ;
#73668=VERTEX_POINT ( 'NONE', #12172 ) ;
#73672=CARTESIAN_POINT ( 'NONE',  ( 20.09692647535021948, 7.048664716645152595, -1.500000000000002220 ) ) ;
#73673=ORIENTED_EDGE ( 'NONE', *, *, #64893, .T. ) ;
#73675=CARTESIAN_POINT ( 'NONE',  ( 21.45948982579844255, -4.128456637845983934, 11.49999999999998934 ) ) ;
#73677=CARTESIAN_POINT ( 'NONE',  ( -10.49914784070103124, -20.09245350529190688, -1.500000000000002220 ) ) ;
#73678=CARTESIAN_POINT ( 'NONE',  ( -41.30067620550419605, -25.28892508720148413, 3.692502541096877700 ) ) ;
#73680=CARTESIAN_POINT ( 'NONE',  ( -8.129759772327192380, 20.32010563749377141, -1.500000000000002220 ) ) ;
#73681=CARTESIAN_POINT ( 'NONE',  ( -62.52287095715006160, -29.50248528299804818, 1.056150453629034924 ) ) ;
#73682=VERTEX_POINT ( 'NONE', #21275 ) ;
#73683=CARTESIAN_POINT ( 'NONE',  ( -39.56136241089613037, -29.50249502162446902, 5.536722193922502200 ) ) ;
#73684=FACE_OUTER_BOUND ( 'NONE', #30100, .T. ) ;
#73687=ORIENTED_EDGE ( 'NONE', *, *, #93926, .F. ) ;
#73689=FACE_OUTER_BOUND ( 'NONE', #8117, .T. ) ;
#73690=CARTESIAN_POINT ( 'NONE',  ( 4.782327729912362990, -20.71560727227588927, -1.500000000000002220 ) ) ;
#73692=CARTESIAN_POINT ( 'NONE',  ( -26.63407156546748311, -24.97064516063613482, 2.799621320528929314 ) ) ;
#73694=EDGE_CURVE ( 'NONE', #40376, #86483, #56163, .T. ) ;
#73695=CARTESIAN_POINT ( 'NONE',  ( -85.62828706649705168, -24.73486907724918282, 1.287355809206962576 ) ) ;
#73696=CARTESIAN_POINT ( 'NONE',  ( -68.58388308116877852, -24.51314013834315375, 0.6176544820404133995 ) ) ;
#73697=CARTESIAN_POINT ( 'NONE',  ( -39.62287095715007723, -24.35013146730202038, 9.818937971375113705 ) ) ;
#73698=VERTEX_POINT ( 'NONE', #42656 ) ;
#73699=CARTESIAN_POINT ( 'NONE',  ( 15.26536572251939461, -12.21375333317339695, 11.49999999999999645 ) ) ;
#73700=CARTESIAN_POINT ( 'NONE',  ( -99.49761415653327390, -25.31438896437989783, 4.819718821452458890 ) ) ;
#73701=CARTESIAN_POINT ( 'NONE',  ( -27.70544111104076990, -24.64017222881049207, 8.251826729410561612 ) ) ;
#73702=ORIENTED_EDGE ( 'NONE', *, *, #64051, .T. ) ;
#73704=LINE ( 'NONE', #4198, #3708 ) ;
#73706=CARTESIAN_POINT ( 'NONE',  ( -99.85057463794808541, -25.31439564997497627, 5.344630366307050018 ) ) ;
#73708=CARTESIAN_POINT ( 'NONE',  ( -81.34205133964172774, -25.03156002429774674, 7.294265505898619217 ) ) ;
#73709=CARTESIAN_POINT ( 'NONE',  ( -11.91260469445801995, 15.66180005371307260, 11.49999999999998934 ) ) ;
#73712=CARTESIAN_POINT ( 'NONE',  ( -111.5228709571500616, -23.47593901973090524, -1.443836447538996204 ) ) ;
#73714=VERTEX_POINT ( 'NONE', #32771 ) ;
#73716=CARTESIAN_POINT ( 'NONE',  ( -125.9228709571500531, -23.47593901973090169, -1.443836447538996426 ) ) ;
#73717=CARTESIAN_POINT ( 'NONE',  ( -55.57061825219870599, -23.48783264082475952, -1.443836473390099462 ) ) ;
#73718=CARTESIAN_POINT ( 'NONE',  ( -118.5181944844509445, -24.34968618360933945, 0.1864209137778906622 ) ) ;
#73719=CARTESIAN_POINT ( 'NONE',  ( -79.92040109509791534, -25.14083923594767356, 2.947789366383930520 ) ) ;
#73720=CARTESIAN_POINT ( 'NONE',  ( -69.34374060353803770, -25.31201778562015647, 6.178485698096741530 ) ) ;
#73721=CARTESIAN_POINT ( 'NONE',  ( -98.62287095715005592, -29.50250243563736774, 8.947779886222138046 ) ) ;
#73722=CARTESIAN_POINT ( 'NONE',  ( 19.80199147212610811, 2.383747631481649254, 11.49999999999998934 ) ) ;
#73724=B_SPLINE_CURVE_WITH_KNOTS ( 'NONE', 3,
 ( #88824, #49771, #64513, #3590 ),
 .UNSPECIFIED., .F., .F.,
 ( 4, 4 ),
 ( 0.000000000000000000, 0.001530649038461520672 ),
 .UNSPECIFIED. ) ;
#73725=CARTESIAN_POINT ( 'NONE',  ( -0.03593141581049384692, -22.58483958596433183, 1.674192380102054178 ) ) ;
#73726=CARTESIAN_POINT ( 'NONE',  ( 4.721227339208565965, -19.33841413273825793, -1.500000000000002220 ) ) ;
#73727=ORIENTED_EDGE ( 'NONE', *, *, #42529, .F. ) ;
#73728=CARTESIAN_POINT ( 'NONE',  ( -29.52287095715006515, -23.38906523657919578, -1.443836447538998424 ) ) ;
#73729=CARTESIAN_POINT ( 'NONE',  ( -29.52287095715006160, -24.57685061924431835, 8.947790457046968626 ) ) ;
#73732=CARTESIAN_POINT ( 'NONE',  ( -26.33488822642538452, -24.89212854592702584, 6.524121854850513991 ) ) ;
#73734=EDGE_CURVE ( 'NONE', #58437, #41257, #22155, .T. ) ;
#73738=EDGE_CURVE ( 'NONE', #4330, #44716, #94669, .T. ) ;
#73739=CARTESIAN_POINT ( 'NONE',  ( -127.5208720400457452, -24.65952944569305316, 1.056160979905707009 ) ) ;
#73740=ORIENTED_EDGE ( 'NONE', *, *, #28629, .T. ) ;
#73741=CARTESIAN_POINT ( 'NONE',  ( 18.82617747125253871, -7.458514806974097411, -1.500000000000002220 ) ) ;
#73744=CARTESIAN_POINT ( 'NONE',  ( -108.5228709571500758, -23.48783264083353473, -1.443836473376470586 ) ) ;
#73745=EDGE_CURVE ( 'NONE', #87999, #56219, #79143, .T. ) ;
#73748=CARTESIAN_POINT ( 'NONE',  ( -79.88644693265914043, -25.30805915561094466, 4.573105107165710947 ) ) ;
#73750=CARTESIAN_POINT ( 'NONE',  ( -19.74138705131307248, -3.616033589355840849, -1.500000000000002220 ) ) ;
#73751=CARTESIAN_POINT ( 'NONE',  ( -14.96386864383857329, 14.77685607883014640, 11.49999999999999645 ) ) ;
#73753=CARTESIAN_POINT ( 'NONE',  ( -70.65050809644763774, -23.85049219812685806, 10.88485053497527311 ) ) ;
#73754=CARTESIAN_POINT ( 'NONE',  ( 15.76968270297436625, 15.47746201419723100, 11.49999999999998934 ) ) ;
#73757=CARTESIAN_POINT ( 'NONE',  ( -55.55620429048338593, -24.99132157543166244, 2.256160258750668834 ) ) ;
#73759=ORIENTED_EDGE ( 'NONE', *, *, #41919, .T. ) ;
#73760=CARTESIAN_POINT ( 'NONE',  ( -72.55406320783903595, -23.96119346886880663, -0.6495511937832121330 ) ) ;
#73761=PLANE ( 'NONE',  #97210 ) ;
#73762=ORIENTED_EDGE ( 'NONE', *, *, #70192, .F. ) ;
#73764=CARTESIAN_POINT ( 'NONE',  ( -63.62287095715004881, -29.50247984919015209, -1.443849546365056913 ) ) ;
#73766=CARTESIAN_POINT ( 'NONE',  ( -76.64820446010540422, -23.48783264082477373, -1.443836473390089026 ) ) ;
#73767=CARTESIAN_POINT ( 'NONE',  ( 20.22723401096548201, -3.897675682603606084, -1.500000000000002220 ) ) ;
#73769=CARTESIAN_POINT ( 'NONE',  ( -5.740839400147730309, 20.75665450205591966, 11.49999999999999645 ) ) ;
#73770=ORIENTED_EDGE ( 'NONE', *, *, #78568, .F. ) ;
#73774=CARTESIAN_POINT ( 'NONE',  ( 13.23790625878087468, -17.95846084735695314, -1.500000000000002220 ) ) ;
#73775=VECTOR ( 'NONE', #81004, 1000.000000000000114 ) ;
#73777=LINE ( 'NONE', #58563, #51310 ) ;
#73779=CARTESIAN_POINT ( 'NONE',  ( -32.62287095715005592, -24.50321055353805022, 9.387540953477529371 ) ) ;
#73781=CARTESIAN_POINT ( 'NONE',  ( 19.25983760003161294, 7.974354923662064998, -1.500000000000002220 ) ) ;
#73782=VERTEX_POINT ( 'NONE', #100253 ) ;
#73784=ORIENTED_EDGE ( 'NONE', *, *, #52858, .F. ) ;
#73787=PLANE ( 'NONE',  #53608 ) ;
#73788=CARTESIAN_POINT ( 'NONE',  ( 21.06685942672242362, 1.161445541649065882, -1.500000000000002220 ) ) ;
#73789=EDGE_LOOP ( 'NONE', ( #61066, #14371, #92834, #27850 ) ) ;
#73790=CARTESIAN_POINT ( 'NONE',  ( -96.52287095715007581, -23.47593901973090524, -1.443836447538996648 ) ) ;
#73791=CARTESIAN_POINT ( 'NONE',  ( -49.51651934166289237, -25.30545405216991028, 5.068386278593029814 ) ) ;
#73792=CARTESIAN_POINT ( 'NONE',  ( -120.6279584262366456, -23.85049219812686871, 10.88485053497526778 ) ) ;
#73793=B_SPLINE_CURVE_WITH_KNOTS ( 'NONE', 3,
 ( #56100, #41877, #70817, #55600, #3325, #62716 ),
 .UNSPECIFIED., .F., .F.,
 ( 4, 2, 4 ),
 ( 0.000000000000000000, 0.001380764517853251419, 0.002761529035706502839 ),
 .UNSPECIFIED. ) ;
#73795=B_SPLINE_CURVE_WITH_KNOTS ( 'NONE', 3,
 ( #99478, #29974, #83265, #53832 ),
 .UNSPECIFIED., .F., .F.,
 ( 4, 4 ),
 ( 0.000000000000000000, 9.999999999998206125E-05 ),
 .UNSPECIFIED. ) ;
#73796=CARTESIAN_POINT ( 'NONE',  ( -129.6228709571500701, -24.33927499327855415, 9.819080762295811837 ) ) ;
#73797=CARTESIAN_POINT ( 'NONE',  ( -18.79206335510377102, -10.79472360063173397, -1.500000000000002220 ) ) ;
#73799=CARTESIAN_POINT ( 'NONE',  ( -20.07822104958740539, -9.643837532803976487, 11.49999999999999645 ) ) ;
#73800=ORIENTED_EDGE ( 'NONE', *, *, #67580, .F. ) ;
#73801=CARTESIAN_POINT ( 'NONE',  ( -76.62287095715007013, -23.47593901973091235, -1.443836447539004642 ) ) ;
#73803=DIRECTION ( 'NONE',  ( 0.000000000000000000, 0.9999999999976377785, 2.173523156925979128E-06 ) ) ;
#73805=CARTESIAN_POINT ( 'NONE',  ( -40.62287095715004881, -24.52232992886363760, 0.6492154411906044809 ) ) ;
#73809=CARTESIAN_POINT ( 'NONE',  ( -100.7114214627874844, -25.13701171212321839, 7.079427678575232363 ) ) ;
#73811=EDGE_CURVE ( 'NONE', #4166, #93720, #17318, .T. ) ;
#73813=CARTESIAN_POINT ( 'NONE',  ( -38.52287095715009713, -24.33832256527048088, 0.1851278514138572362 ) ) ;
#73814=ORIENTED_EDGE ( 'NONE', *, *, #25652, .T. ) ;
#73815=CARTESIAN_POINT ( 'NONE',  ( -130.5728709571500588, -25.24367434374222086, 7.008680551007247850 ) ) ;
#73816=CARTESIAN_POINT ( 'NONE',  ( 21.09243369641204069, 7.689775423913054908, -1.500000000000002220 ) ) ;
#73819=CARTESIAN_POINT ( 'NONE',  ( -100.3502092750176047, -25.04369193928073045, 7.560303740803074213 ) ) ;
#73820=CARTESIAN_POINT ( 'NONE',  ( -101.5575535147763162, -23.73791477778911840, 11.05961554403170588 ) ) ;
#73823=EDGE_CURVE ( 'NONE', #7140, #20070, #14980, .T. ) ;
#73825=EDGE_CURVE ( 'NONE', #53278, #57950, #14783, .T. ) ;
#73826=CARTESIAN_POINT ( 'NONE',  ( -130.5728709571500588, -24.57215472537219014, 9.174899246800711339 ) ) ;
#73827=CARTESIAN_POINT ( 'NONE',  ( -9.247272915838292917, -17.29429475886123768, 11.49999999999998934 ) ) ;
#73828=B_SPLINE_CURVE_WITH_KNOTS ( 'NONE', 3,
 ( #28893, #90796, #13155, #82178 ),
 .UNSPECIFIED., .F., .F.,
 ( 4, 4 ),
 ( 0.000000000000000000, 9.999999999998897304E-05 ),
 .UNSPECIFIED. ) ;
#73829=DIRECTION ( 'NONE',  ( 0.000000000000000000, -2.173523156925979552E-06, 0.9999999999976378895 ) ) ;
#73831=ADVANCED_FACE ( 'NONE', ( #24154 ), #9428, .F. ) ;
#73832=CARTESIAN_POINT ( 'NONE',  ( 16.61460563260716583, 13.71664681387569118, -1.500000000000002220 ) ) ;
#73834=FACE_OUTER_BOUND ( 'NONE', #31198, .T. ) ;
#73836=DIRECTION ( 'NONE',  ( 2.567145104890970367E-18, -0.9999999999976378895, -2.173523156893722419E-06 ) ) ;
#73837=CARTESIAN_POINT ( 'NONE',  ( 22.26416322464526232, -5.798680748638591176, -1.500000000000002220 ) ) ;
#73840=CARTESIAN_POINT ( 'NONE',  ( -107.5228709571500758, -29.50248528299804818, 1.056150453629043584 ) ) ;
#73841=CARTESIAN_POINT ( 'NONE',  ( -49.58723797677291856, -24.34968618360933590, 0.1864209137778799763 ) ) ;
#73842=CARTESIAN_POINT ( 'NONE',  ( -7.807601069497579260, -18.53474111305376937, 11.49999999999999645 ) ) ;
#73843=CARTESIAN_POINT ( 'NONE',  ( -39.62287095715005592, -29.50248528299804818, 1.056150453629031594 ) ) ;
#73844=CARTESIAN_POINT ( 'NONE',  ( -89.62287095715004170, -24.65952944569305316, 1.056160979905700348 ) ) ;
#73850=CARTESIAN_POINT ( 'NONE',  ( -18.79335158860655142, 6.462138572525057967, 11.49999999999998934 ) ) ;
#73853=CARTESIAN_POINT ( 'NONE',  ( -113.5190820818342132, -23.96119346886881019, -0.6495511937832028071 ) ) ;
#73854=CARTESIAN_POINT ( 'NONE',  ( 15.33752688427012778, 12.42672799324400934, -1.500000000000002220 ) ) ;
#73856=CARTESIAN_POINT ( 'NONE',  ( -90.30662908837275893, -25.33592526241815790, 4.020882415642697438 ) ) ;
#73860=CARTESIAN_POINT ( 'NONE',  ( 14.37238272058661259, 14.81585024043302035, 11.49999999999999645 ) ) ;
#73862=LINE ( 'NONE', #65284, #49673 ) ;
#73863=CARTESIAN_POINT ( 'NONE',  ( -1.322449806865925614, 22.60218017400935864, 11.49999999999999645 ) ) ;
#73864=VERTEX_POINT ( 'NONE', #10942 ) ;
#73865=CARTESIAN_POINT ( 'NONE',  ( -129.6228709571500133, -23.48783264082478794, -1.443836473390056607 ) ) ;
#73870=ORIENTED_EDGE ( 'NONE', *, *, #4350, .F. ) ;
#73871=ADVANCED_FACE ( 'NONE', ( #19044 ), #49013, .T. ) ;
#73872=VERTEX_POINT ( 'NONE', #41908 ) ;
#73873=CARTESIAN_POINT ( 'NONE',  ( -99.31360333396543183, -25.23370691691098600, 6.322973554867211021 ) ) ;
#73874=CARTESIAN_POINT ( 'NONE',  ( -4.526818761702180893, -22.41603498850323817, 11.49999999999998934 ) ) ;
#73876=EDGE_CURVE ( 'NONE', #21078, #96665, #87563, .T. ) ;
#73877=CARTESIAN_POINT ( 'NONE',  ( -19.35566633068252074, -9.524217769563914970, -1.500000000000002220 ) ) ;
#73879=LINE ( 'NONE', #4869, #46864 ) ;
#73880=B_SPLINE_CURVE_WITH_KNOTS ( 'NONE', 3,
 ( #57133, #58617, #33776, #65747 ),
 .UNSPECIFIED., .F., .F.,
 ( 4, 4 ),
 ( 0.8894174519954087810, 0.8904181990361742516 ),
 .UNSPECIFIED. ) ;
#73881=CARTESIAN_POINT ( 'NONE',  ( -1.585881643086899606, 22.48459252949185228, 11.49999999999999645 ) ) ;
#73883=CARTESIAN_POINT ( 'NONE',  ( -43.62370908719063323, -24.65952944569304606, 1.056160979905693909 ) ) ;
#73884=CARTESIAN_POINT ( 'NONE',  ( 0.3405503412851532130, 21.98688381012616233, 11.49999999999998934 ) ) ;
#73885=CARTESIAN_POINT ( 'NONE',  ( -111.5172671840988983, -24.15543982623907482, -0.2315651400026575712 ) ) ;
#73886=DIRECTION ( 'NONE',  ( -0.000000000000000000, 2.173523156925979552E-06, -0.9999999999976378895 ) ) ;
#73887=ORIENTED_EDGE ( 'NONE', *, *, #66769, .T. ) ;
#73888=EDGE_CURVE ( 'NONE', #60977, #82121, #72863, .T. ) ;
#73889=CARTESIAN_POINT ( 'NONE',  ( -63.62287095715004881, -24.64965695001468404, 8.947790433994185832 ) ) ;
#73892=CARTESIAN_POINT ( 'NONE',  ( -77.62287095715005592, -24.64898659630367916, 1.056161002820826145 ) ) ;
#73893=VERTEX_POINT ( 'NONE', #34286 ) ;
#73894=VERTEX_POINT ( 'NONE', #50503 ) ;
#73895=ORIENTED_EDGE ( 'NONE', *, *, #55396, .F. ) ;
#73896=LINE ( 'NONE', #58672, #24262 ) ;
#73898=CARTESIAN_POINT ( 'NONE',  ( -64.52287095715006160, -23.47596703998600631, 11.44779298504228926 ) ) ;
#73899=CARTESIAN_POINT ( 'NONE',  ( 0.5039804632396667206, -20.40334623801319580, -1.500000000000002220 ) ) ;
#73900=VERTEX_POINT ( 'NONE', #88569 ) ;
#73902=CARTESIAN_POINT ( 'NONE',  ( -29.58658507105814195, -24.27136956112387267, 9.817618405055078767 ) ) ;
#73904=LINE ( 'NONE', #36343, #46490 ) ;
#73905=CARTESIAN_POINT ( 'NONE',  ( -71.18291627536595456, -25.25855322842343753, 7.291244491205598699 ) ) ;
#73906=ORIENTED_EDGE ( 'NONE', *, *, #1330, .F. ) ;
#73907=CARTESIAN_POINT ( 'NONE',  ( -28.10168127693285101, -24.76880867787903284, 2.337527702696277743 ) ) ;
#73908=CARTESIAN_POINT ( 'NONE',  ( -33.58953762381673158, -24.65952944569304250, 1.056160979905696351 ) ) ;
#73910=CARTESIAN_POINT ( 'NONE',  ( -4.307737697753418082, 20.33289072680551968, 11.49999999999998934 ) ) ;
#73912=PLANE ( 'NONE',  #29637 ) ;
#73913=VERTEX_POINT ( 'NONE', #73346 ) ;
#73914=VECTOR ( 'NONE', #29199, 1000.000000000000114 ) ;
#73915=B_SPLINE_CURVE_WITH_KNOTS ( 'NONE', 3,
 ( #77283, #54974, #9280, #14891, #38232, #40245 ),
 .UNSPECIFIED., .F., .F.,
 ( 4, 2, 4 ),
 ( 1.570755371634170283E-05, 0.001396183895866089054, 0.002776660238015836446 ),
 .UNSPECIFIED. ) ;
#73916=DIRECTION ( 'NONE',  ( -0.000000000000000000, 2.173523156925979552E-06, -0.9999999999976378895 ) ) ;
#73918=ORIENTED_EDGE ( 'NONE', *, *, #99643, .T. ) ;
#73919=EDGE_LOOP ( 'NONE', ( #65472, #13974, #4008, #88420 ) ) ;
#73920=AXIS2_PLACEMENT_3D ( 'NONE', #54347, #16765, #94396 ) ;
#73921=B_SPLINE_CURVE_WITH_KNOTS ( 'NONE', 3,
 ( #3787, #65698, #41340, #26110, #73779, #18989 ),
 .UNSPECIFIED., .F., .F.,
 ( 4, 2, 4 ),
 ( 0.000000000000000000, 0.001380901958385381606, 0.002761803916770763211 ),
 .UNSPECIFIED. ) ;
#73922=LINE ( 'NONE', #59203, #34886 ) ;
#73923=CARTESIAN_POINT ( 'NONE',  ( -77.62287095715005592, -24.64965695001468404, 8.947790433994182280 ) ) ;
#73924=AXIS2_PLACEMENT_3D ( 'NONE', #19914, #96546, #18918 ) ;
#73925=CARTESIAN_POINT ( 'NONE',  ( -101.1944152955115186, -25.17323144036708626, 6.858246026757193192 ) ) ;
#73926=CARTESIAN_POINT ( 'NONE',  ( -43.56914089629323428, -23.48786465467240347, 11.44779295918255180 ) ) ;
#73927=CARTESIAN_POINT ( 'NONE',  ( 10.35204687333978057, 19.51823071965408829, 11.49999999999999645 ) ) ;
#73930=PLANE ( 'NONE',  #65115 ) ;
#73931=CARTESIAN_POINT ( 'NONE',  ( -13.31036990564671818, -18.29084955798148471, -1.500000000000002220 ) ) ;
#73932=AXIS2_PLACEMENT_3D ( 'NONE', #82597, #44037, #12583 ) ;
#73933=CARTESIAN_POINT ( 'NONE',  ( -115.6262966384274620, -24.52399227489127043, 9.353111116836528183 ) ) ;
#73939=CARTESIAN_POINT ( 'NONE',  ( -82.62287095715005592, -29.50247984919015209, -1.443849546365053582 ) ) ;
#73940=ORIENTED_EDGE ( 'NONE', *, *, #23902, .F. ) ;
#73941=CARTESIAN_POINT ( 'NONE',  ( -12.03079493616482765, -17.41531974249929249, 11.49999999999998934 ) ) ;
#73944=CARTESIAN_POINT ( 'NONE',  ( -80.62287095715007013, -24.63345952396257488, 9.038047939301510070 ) ) ;
#73945=CARTESIAN_POINT ( 'NONE',  ( 19.83320176327591255, -10.20924650237717835, -1.500000000000002220 ) ) ;
#73946=EDGE_CURVE ( 'NONE', #68625, #30205, #65258, .T. ) ;
#73948=EDGE_CURVE ( 'NONE', #52488, #6180, #89563, .T. ) ;
#73949=ORIENTED_EDGE ( 'NONE', *, *, #300, .F. ) ;
#73952=ADVANCED_FACE ( 'NONE', ( #80953 ), #42416, .T. ) ;
#73955=CARTESIAN_POINT ( 'NONE',  ( -83.52287095715006160, -24.64965694238407323, 8.947790433994198267 ) ) ;
#73956=CARTESIAN_POINT ( 'NONE',  ( 1.133552453683672745, -19.47370032599940615, 11.49999999999998934 ) ) ;
#73957=CARTESIAN_POINT ( 'NONE',  ( 15.63241172484657682, -14.69700884395465934, 11.49999999999998934 ) ) ;
#73958=CARTESIAN_POINT ( 'NONE',  ( -26.06135888742384665, -24.57999700124051756, 2.563275948977453922 ) ) ;
#73959=CARTESIAN_POINT ( 'NONE',  ( -107.6228709571500701, -23.48786465467241769, 11.44779295918253936 ) ) ;
#73960=CARTESIAN_POINT ( 'NONE',  ( -77.55022051755103973, -24.15543982623907482, -0.2315651400026658147 ) ) ;
#73961=CARTESIAN_POINT ( 'NONE',  ( 17.57702471007113232, 14.52005670271990034, -1.500000000000002220 ) ) ;
#73963=CARTESIAN_POINT ( 'NONE',  ( -106.5947057434380554, -23.73791477778912551, 11.05961554403169878 ) ) ;
#73965=CARTESIAN_POINT ( 'NONE',  ( -16.62890364678930410, -10.96057169749504645, 11.49999999999999645 ) ) ;
#73966=CARTESIAN_POINT ( 'NONE',  ( -104.5154284841441950, -24.15543982623907482, -0.2315651400026580709 ) ) ;
#73968=CARTESIAN_POINT ( 'NONE',  ( -128.5895376238167103, -24.66019654487200086, 8.947790411086117501 ) ) ;
#73970=CARTESIAN_POINT ( 'NONE',  ( -118.6228709571500701, -23.47596703998600631, 11.44779298504227683 ) ) ;
#73971=EDGE_CURVE ( 'NONE', #13108, #70610, #95177, .T. ) ;
#73972=CARTESIAN_POINT ( 'NONE',  ( -31.80983992280592787, -25.31516574674648368, 3.894478520810415567 ) ) ;
#73973=CARTESIAN_POINT ( 'NONE',  ( -9.282276271697774916, -19.63344595494797673, -1.500000000000002220 ) ) ;
#73975=CARTESIAN_POINT ( 'NONE',  ( -5.499840656826012975, 18.73951620154120334, -1.500000000000002220 ) ) ;
#73977=CARTESIAN_POINT ( 'NONE',  ( -55.64835622778738156, -24.15602025860896518, 10.28564288303535257 ) ) ;
#73978=B_SPLINE_CURVE_WITH_KNOTS ( 'NONE', 3,
 ( #43750, #36133, #59980, #67103 ),
 .UNSPECIFIED., .F., .F.,
 ( 4, 4 ),
 ( 0.000000000000000000, 9.999999999998897304E-05 ),
 .UNSPECIFIED. ) ;
#73983=CARTESIAN_POINT ( 'NONE',  ( 2.691128592823461840, 20.25793168094256202, 11.49999999999999645 ) ) ;
#73985=AXIS2_PLACEMENT_3D ( 'NONE', #50294, #89840, #73623 ) ;
#73986=PLANE ( 'NONE',  #44802 ) ;
#73987=EDGE_LOOP ( 'NONE', ( #91998, #18592, #33708, #87116 ) ) ;
#73988=DIRECTION ( 'NONE',  ( 0.000000000000000000, -0.9999999999976377785, -2.173523156925979128E-06 ) ) ;
#73993=B_SPLINE_CURVE_WITH_KNOTS ( 'NONE', 3,
 ( #17623, #24723, #40468, #1908 ),
 .UNSPECIFIED., .F., .F.,
 ( 4, 4 ),
 ( 0.000000000000000000, 9.999999999999592548E-05 ),
 .UNSPECIFIED. ) ;
#73994=DIRECTION ( 'NONE',  ( -3.773278334453079618E-23, 0.9999999999976377785, 2.173523156925978705E-06 ) ) ;
#73997=VECTOR ( 'NONE', #99175, 1000.000000000000114 ) ;
#73999=CARTESIAN_POINT ( 'NONE',  ( 9.898807498884217182, 20.75630955806377287, 11.49999999999999645 ) ) ;
#74000=CARTESIAN_POINT ( 'NONE',  ( -20.37646751746074969, -10.17465561509698979, -1.500000000000002220 ) ) ;
#74001=CARTESIAN_POINT ( 'NONE',  ( -110.5858253176389212, -25.00182538069147498, 7.747789668545046027 ) ) ;
#74004=CARTESIAN_POINT ( 'NONE',  ( -49.62287095715005592, -24.64898659630528499, 1.056161002820821038 ) ) ;
#74005=CARTESIAN_POINT ( 'NONE',  ( -54.52287095715006870, -23.48786465467240347, 11.44779295918255002 ) ) ;
#74007=CARTESIAN_POINT ( 'NONE',  ( -21.73523922981167189, -2.474665994198115726, -1.500000000000002220 ) ) ;
#74009=PLANE ( 'NONE',  #43637 ) ;
#74011=ORIENTED_EDGE ( 'NONE', *, *, #22848, .F. ) ;
#74012=CARTESIAN_POINT ( 'NONE',  ( -15.93830457579706739, -12.76012858937699335, 11.49999999999998934 ) ) ;
#74015=ORIENTED_EDGE ( 'NONE', *, *, #29498, .F. ) ;
#74017=CARTESIAN_POINT ( 'NONE',  ( 22.18053613645642841, 6.281410551025238043, -1.500000000000002220 ) ) ;
#74018=CARTESIAN_POINT ( 'NONE',  ( -80.52287095715006160, -23.85196035786901092, -0.8779234886475191235 ) ) ;
#74019=CARTESIAN_POINT ( 'NONE',  ( -8.513533612778267923, 18.29693335657625042, -1.500000000000002220 ) ) ;
#74020=EDGE_LOOP ( 'NONE', ( #79001, #55411, #55031, #67170 ) ) ;
#74022=CARTESIAN_POINT ( 'NONE',  ( -98.62287095715007013, -23.47596703998600631, 11.44779298504227860 ) ) ;
#74023=CARTESIAN_POINT ( 'NONE',  ( -40.94688081444584782, -25.03284417894045788, 7.563176522466704910 ) ) ;
#74024=LINE ( 'NONE', #26847, #64154 ) ;
#74026=CARTESIAN_POINT ( 'NONE',  ( 18.17913347391500523, 11.28257676469832660, 11.49999999999999645 ) ) ;
#74027=ORIENTED_EDGE ( 'NONE', *, *, #9163, .T. ) ;
#74028=LINE ( 'NONE', #4523, #1475 ) ;
#74031=CARTESIAN_POINT ( 'NONE',  ( -13.70410651198969809, -17.55484038775568933, -1.500000000000002220 ) ) ;
#74032=B_SPLINE_CURVE_WITH_KNOTS ( 'NONE', 3,
 ( #30843, #9005, #47584, #39958 ),
 .UNSPECIFIED., .F., .F.,
 ( 4, 4 ),
 ( 0.000000000000000000, 0.0001000000000000167422 ),
 .UNSPECIFIED. ) ;
#74033=CARTESIAN_POINT ( 'NONE',  ( 20.68991284688621946, 0.5745778482356619365, -1.500000000000002220 ) ) ;
#74034=VERTEX_POINT ( 'NONE', #6318 ) ;
#74035=FACE_OUTER_BOUND ( 'NONE', #73320, .T. ) ;
#74036=ORIENTED_EDGE ( 'NONE', *, *, #94187, .T. ) ;
#74037=CARTESIAN_POINT ( 'NONE',  ( -56.52287095715007581, -23.72747288104470087, -1.053458166803226570 ) ) ;
#74038=ORIENTED_EDGE ( 'NONE', *, *, #47858, .T. ) ;
#74040=CARTESIAN_POINT ( 'NONE',  ( 2.438461900574103502, 20.79476225230834174, -1.500000000000002220 ) ) ;
#74041=CARTESIAN_POINT ( 'NONE',  ( -16.30586240431254197, 14.59307310709210626, 11.49999999999999645 ) ) ;
#74042=CARTESIAN_POINT ( 'NONE',  ( -37.53288840155523332, -24.51419770103156637, 9.386484678747175181 ) ) ;
#74043=CARTESIAN_POINT ( 'NONE',  ( 9.939345090160914609, -20.19931669485651682, -1.500000000000002220 ) ) ;
#74045=CARTESIAN_POINT ( 'NONE',  ( 13.96602909953038640, 15.60522523583095200, -1.500000000000002220 ) ) ;
#74046=CARTESIAN_POINT ( 'NONE',  ( -26.09636659181000695, -24.97066789626643413, 4.940287549524292388 ) ) ;
#74048=CARTESIAN_POINT ( 'NONE',  ( -119.6264748175326105, -23.96169478059714564, 10.65365249895717170 ) ) ;
#74052=EDGE_LOOP ( 'NONE', ( #50714, #10341, #9902, #79334 ) ) ;
#74053=CARTESIAN_POINT ( 'NONE',  ( -91.52287095715006160, -29.50250243563736774, 8.947779886222139822 ) ) ;
#74054=ORIENTED_EDGE ( 'NONE', *, *, #69521, .T. ) ;
#74056=CARTESIAN_POINT ( 'NONE',  ( 5.910897418159350103, -20.63055655796343757, -1.500000000000002220 ) ) ;
#74057=ADVANCED_FACE ( 'NONE', ( #35781 ), #30480, .T. ) ;
#74058=CARTESIAN_POINT ( 'NONE',  ( -51.93149462243455616, -25.25905089634592571, 6.174051128686508072 ) ) ;
#74061=CARTESIAN_POINT ( 'NONE',  ( 19.97611676871187569, -6.800378171449690257, -1.500000000000002220 ) ) ;
#74062=CARTESIAN_POINT ( 'NONE',  ( -87.52287095715006160, -24.64898659630528854, 1.056161002820827921 ) ) ;
#74065=CARTESIAN_POINT ( 'NONE',  ( -97.52287095715006160, -23.47596703998600631, 11.44779298504228215 ) ) ;
#74066=AXIS2_PLACEMENT_3D ( 'NONE', #78515, #56216, #87145 ) ;
#74068=CARTESIAN_POINT ( 'NONE',  ( -100.5562042904833788, -24.99132157543166599, 2.256160258750667058 ) ) ;
#74069=CARTESIAN_POINT ( 'NONE',  ( 20.57361055066190758, -8.084994430987380909, -1.500000000000002220 ) ) ;
#74070=CARTESIAN_POINT ( 'NONE',  ( -116.5158267652437729, -24.65952944569305316, 1.056160979905712338 ) ) ;
#74073=CARTESIAN_POINT ( 'NONE',  ( -40.89894032811586300, -25.31624730604892903, 5.492539635573550960 ) ) ;
#74074=B_SPLINE_CURVE_WITH_KNOTS ( 'NONE', 3,
 ( #9448, #96197, #25168, #72864, #71863, #26176, #72363, #24662 ),
 .UNSPECIFIED., .F., .F.,
 ( 4, 2, 2, 4 ),
 ( -0.001224554619866345846, -0.0002241820295893650998, 0.0007761905606876156466, 0.002776935741241582344 ),
 .UNSPECIFIED. ) ;
#74075=EDGE_CURVE ( 'NONE', #55313, #76664, #59125, .T. ) ;
#74076=CARTESIAN_POINT ( 'NONE',  ( -62.54342312881265542, -24.35071581493542681, 9.817618358456032368 ) ) ;
#74079=CARTESIAN_POINT ( 'NONE',  ( 16.79701800048795590, -13.18750964578662455, 11.49999999999998934 ) ) ;
#74081=EDGE_CURVE ( 'NONE', #40482, #67931, #21032, .T. ) ;
#74082=CARTESIAN_POINT ( 'NONE',  ( -48.86261576302199217, -25.03707831087709579, 7.590867751134624974 ) ) ;
#74083=DIRECTION ( 'NONE',  ( 0.000000000000000000, -0.9999999999976377785, -2.173523156925979128E-06 ) ) ;
#74084=DIRECTION ( 'NONE',  ( 1.000000000000000000, 3.773278334444167608E-23, 8.201307833595939069E-29 ) ) ;
#74085=CARTESIAN_POINT ( 'NONE',  ( 14.05383982582471170, -17.77673030755399708, -1.500000000000002220 ) ) ;
#74088=CARTESIAN_POINT ( 'NONE',  ( -50.37830952628071657, -25.31401921878212136, 5.197788989978542773 ) ) ;
#74089=CARTESIAN_POINT ( 'NONE',  ( -79.51272270944330955, -23.96119346886880308, -0.6495511937832122440 ) ) ;
#74090=CARTESIAN_POINT ( 'NONE',  ( 7.891737972721761807, -18.10977644326358771, 11.49999999999999645 ) ) ;
#74091=LINE ( 'NONE', #97902, #48841 ) ;
#74092=CARTESIAN_POINT ( 'NONE',  ( -73.52287095715007581, -23.72773821059537269, 11.05748984161097503 ) ) ;
#74094=DIRECTION ( 'NONE',  ( -3.773278334453079030E-23, 0.9999999999976377785, 2.173523156925979128E-06 ) ) ;
#74096=CARTESIAN_POINT ( 'NONE',  ( -101.0369185477202336, -25.17353314354872396, 6.965963161511662172 ) ) ;
#74097=CARTESIAN_POINT ( 'NONE',  ( -9.004746288917990782, -19.65190454534591069, 11.49999999999998934 ) ) ;
#74098=AXIS2_PLACEMENT_3D ( 'NONE', #70041, #527, #9644 ) ;
#74099=CARTESIAN_POINT ( 'NONE',  ( -70.62287095715005592, -29.50249982740957577, 7.747779886224967605 ) ) ;
#74100=CARTESIAN_POINT ( 'NONE',  ( -81.42380231474228935, -25.30401792888237011, 5.197789011716578145 ) ) ;
#74101=CARTESIAN_POINT ( 'NONE',  ( -45.62287095715004881, -29.50250243563736774, 8.947779886222146928 ) ) ;
#74102=CARTESIAN_POINT ( 'NONE',  ( 14.45944668481935658, 13.51102189132778442, -1.500000000000002220 ) ) ;
#74104=VECTOR ( 'NONE', #4325, 1000.000000000000114 ) ;
#74105=CARTESIAN_POINT ( 'NONE',  ( 16.58868386459195676, 11.68684615565071283, 11.49999999999999645 ) ) ;
#74106=FACE_OUTER_BOUND ( 'NONE', #20924, .T. ) ;
#74107=CARTESIAN_POINT ( 'NONE',  ( -44.52287095715004739, -24.51283580621364777, 0.6167428607019598275 ) ) ;
#74108=ORIENTED_EDGE ( 'NONE', *, *, #17399, .F. ) ;
#74111=DIRECTION ( 'NONE',  ( 3.773278334444167608E-23, -1.000000000000000000, 0.000000000000000000 ) ) ;
#74112=CARTESIAN_POINT ( 'NONE',  ( -95.62287095715007013, -24.92579138211020151, 1.929029949965665569 ) ) ;
#74114=CARTESIAN_POINT ( 'NONE',  ( 7.329891291799937925, -18.66831812819665970, -1.500000000000002220 ) ) ;
#74115=CARTESIAN_POINT ( 'NONE',  ( -67.55620429048337883, -23.48783264082478084, -1.443836473390066377 ) ) ;
#74119=CARTESIAN_POINT ( 'NONE',  ( -127.5228709571500616, -24.64898659630368627, 1.056161002820834804 ) ) ;
#74125=EDGE_CURVE ( 'NONE', #74478, #49573, #86147, .T. ) ;
#74126=CARTESIAN_POINT ( 'NONE',  ( -100.9401440129433070, -25.03707831087709934, 7.590867751134624086 ) ) ;
#74129=CARTESIAN_POINT ( 'NONE',  ( -18.18203184671642703, 9.085611141607108365, -1.500000000000002220 ) ) ;
#74131=CARTESIAN_POINT ( 'NONE',  ( -20.38739128398232836, 10.50225141308550292, -1.500000000000002220 ) ) ;
#74133=ORIENTED_EDGE ( 'NONE', *, *, #4195, .F. ) ;
#74135=CARTESIAN_POINT ( 'NONE',  ( -76.52287095715007581, -23.47593901973090169, -1.443836447538996648 ) ) ;
#74136=CARTESIAN_POINT ( 'NONE',  ( -117.6228709571500559, -23.48786465467241769, 11.44779295918253759 ) ) ;
#74137=CARTESIAN_POINT ( 'NONE',  ( -4.771770383141621608, -20.67029057396967318, 11.49999999999999645 ) ) ;
#74138=B_SPLINE_CURVE_WITH_KNOTS ( 'NONE', 3,
 ( #35712, #27603, #50436, #81879 ),
 .UNSPECIFIED., .F., .F.,
 ( 4, 4 ),
 ( 0.8711220469307209280, 0.8801284782028364617 ),
 .UNSPECIFIED. ) ;
#74139=ORIENTED_EDGE ( 'NONE', *, *, #35818, .T. ) ;
#74140=CARTESIAN_POINT ( 'NONE',  ( -12.04397493737346991, 18.63154960201688226, -1.500000000000002220 ) ) ;
#74141=CARTESIAN_POINT ( 'NONE',  ( 20.46650637700042097, -2.330123182410055893, -1.500000000000002220 ) ) ;
#74143=EDGE_LOOP ( 'NONE', ( #4021, #87113, #22215, #42467 ) ) ;
#74146=CARTESIAN_POINT ( 'NONE',  ( -50.52287095715006160, -24.62285846331433703, 9.038163153548369522 ) ) ;
#74147=ORIENTED_EDGE ( 'NONE', *, *, #59749, .F. ) ;
#74148=ORIENTED_EDGE ( 'NONE', *, *, #7730, .T. ) ;
#74149=ORIENTED_EDGE ( 'NONE', *, *, #8120, .T. ) ;
#74150=FACE_OUTER_BOUND ( 'NONE', #74162, .T. ) ;
#74151=CARTESIAN_POINT ( 'NONE',  ( -28.64431595215229720, -24.00349382954137667, 10.23563545308467049 ) ) ;
#74152=FACE_OUTER_BOUND ( 'NONE', #26108, .T. ) ;
#74153=CARTESIAN_POINT ( 'NONE',  ( -13.51810693421681719, -15.76408947421354156, -1.500000000000002220 ) ) ;
#74154=CARTESIAN_POINT ( 'NONE',  ( 14.84582651547613352, 15.88809324551894520, 11.49999999999999645 ) ) ;
#74155=ORIENTED_EDGE ( 'NONE', *, *, #88448, .T. ) ;
#74156=CARTESIAN_POINT ( 'NONE',  ( -37.62287095715005592, -24.66019654487199020, 8.947790411086135265 ) ) ;
#74159=CARTESIAN_POINT ( 'NONE',  ( -19.78178409256797465, 10.57734301857266246, -1.500000000000002220 ) ) ;
#74161=CARTESIAN_POINT ( 'NONE',  ( -102.5228709571500758, -23.48786465467241769, 11.44779295918254114 ) ) ;
#74162=EDGE_LOOP ( 'NONE', ( #89396, #83878, #93655, #51599 ) ) ;
#74163=CARTESIAN_POINT ( 'NONE',  ( -48.52287095715006160, -29.50250243563736774, 8.947779886222146928 ) ) ;
#74164=CARTESIAN_POINT ( 'NONE',  ( -116.4728709571500502, -25.21113200442380275, 5.000950865234348619 ) ) ;
#74165=B_SPLINE_SURFACE_WITH_KNOTS ( 'NONE', 3, 3, ( 
 ( #100340, #79023, #39474, #63840 ),
 ( #9020, #24242, #17128, #17635 ),
 ( #78012, #911, #39970, #32866 ),
 ( #94252, #31865, #69422, #48097 ),
 ( #54710, #1921, #38966, #8017 ),
 ( #9521, #30856, #94753, #47598 ),
 ( #55216, #77517, #70934, #62834 ) ),
 .UNSPECIFIED., .F., .F., .F.,
 ( 4, 3, 4 ),
 ( 4, 4 ),
 ( 0.7945040050992251413, 0.8970133687736510097, 0.9995227324480769893 ),
 ( 0.8797175456623916867, 0.8811364062137666542 ),
 .UNSPECIFIED. ) ;
#74166=ORIENTED_EDGE ( 'NONE', *, *, #20583, .F. ) ;
#74168=CARTESIAN_POINT ( 'NONE',  ( -46.49380392490311920, -24.35071581493542325, 9.817618358456032368 ) ) ;
#74169=ORIENTED_EDGE ( 'NONE', *, *, #85648, .T. ) ;
#74170=CARTESIAN_POINT ( 'NONE',  ( -19.37389216307569129, 8.798533688548827669, -1.500000000000002220 ) ) ;
#74172=CARTESIAN_POINT ( 'NONE',  ( -88.54557060015829961, -24.51314013834315375, 0.6176544820404129554 ) ) ;
#74174=CARTESIAN_POINT ( 'NONE',  ( 16.27406392464308027, 14.57352745747340172, -1.500000000000002220 ) ) ;
#74176=CARTESIAN_POINT ( 'NONE',  ( -12.60694655700363143, 18.86142483545513926, 11.49999999999998934 ) ) ;
#74177=CARTESIAN_POINT ( 'NONE',  ( -40.45829750704998418, -25.18430871329344711, 3.293943118056679165 ) ) ;
#74179=CARTESIAN_POINT ( 'NONE',  ( 20.11839708684271244, 8.774209887332036217, -1.500000000000002220 ) ) ;
#74180=LINE ( 'NONE', #73681, #90069 ) ;
#74182=B_SPLINE_CURVE_WITH_KNOTS ( 'NONE', 3,
 ( #15096, #22191, #30316, #46062, #85605, #373, #46554, #61292, #45064, #69388 ),
 .UNSPECIFIED., .F., .F.,
 ( 4, 2, 2, 2, 4 ),
 ( 8.673617379884035472E-19, 0.0002559089097569039288, 0.0005118178195138069903, 0.0007677267292707100517, 0.001023635639027613113 ),
 .UNSPECIFIED. ) ;
#74183=CARTESIAN_POINT ( 'NONE',  ( -122.5201542580532248, -24.15620529776629510, 10.23563542870659582 ) ) ;
#74184=CARTESIAN_POINT ( 'NONE',  ( -49.00533630786537032, -25.26337435419707589, 6.749865916534812271 ) ) ;
#74185=ADVANCED_FACE ( 'NONE', ( #61624 ), #93534, .F. ) ;
#74186=VECTOR ( 'NONE', #93402, 1000.000000000000114 ) ;
#74187=EDGE_CURVE ( 'NONE', #34234, #83477, #57245, .T. ) ;
#74191=CARTESIAN_POINT ( 'NONE',  ( -97.52287095715006160, -29.50250243563736774, 8.947779886222138046 ) ) ;
#74192=CARTESIAN_POINT ( 'NONE',  ( -30.60533150986764284, -24.66488071993808617, 1.095224832288503203 ) ) ;
#74193=CARTESIAN_POINT ( 'NONE',  ( 10.81949470224598997, -18.29866561848832518, 11.49999999999998934 ) ) ;
#74194=CARTESIAN_POINT ( 'NONE',  ( -112.5540321080100057, -24.15543982623908192, -0.2315651400026420004 ) ) ;
#74199=CARTESIAN_POINT ( 'NONE',  ( -68.58782206624864841, -24.34968618360933590, 0.1864209137778813363 ) ) ;
#74200=CARTESIAN_POINT ( 'NONE',  ( -32.52287095715004739, -23.47593901973090169, -1.443836447538997092 ) ) ;
#74202=CARTESIAN_POINT ( 'NONE',  ( 7.829539893445508270, 17.95258299782629408, 11.49999999999999645 ) ) ;
#74203=CARTESIAN_POINT ( 'NONE',  ( -43.52287095715007581, -23.47593901973090169, -1.443836447538997092 ) ) ;
#74205=CARTESIAN_POINT ( 'NONE',  ( -28.34266632056247204, -24.71873428796616068, 8.144582237604435448 ) ) ;
#74210=CARTESIAN_POINT ( 'NONE',  ( -63.22287095715005734, -23.47596703998600631, 11.44779298504227683 ) ) ;
#74211=CARTESIAN_POINT ( 'NONE',  ( -62.52287095715006160, -23.48783264082477018, -1.443836473390091912 ) ) ;
#74212=CARTESIAN_POINT ( 'NONE',  ( -0.7274468246531539117, 19.66889477801398911, 11.49999999999998934 ) ) ;
#74215=CARTESIAN_POINT ( 'NONE',  ( -71.30457154551152144, -25.24554880456021522, 6.209207408033732278 ) ) ;
#74217=EDGE_LOOP ( 'NONE', ( #67370, #78173, #19869, #61850 ) ) ;
#74218=CARTESIAN_POINT ( 'NONE',  ( -74.52287095715007581, -23.73907113216989728, -1.053371485793254569 ) ) ;
#74220=CARTESIAN_POINT ( 'NONE',  ( -47.56045512770388228, -23.73766607897670866, -1.055555164236438692 ) ) ;
#74224=DIRECTION ( 'NONE',  ( -3.773278334453079618E-23, 0.9999999999976377785, 2.173523156925979975E-06 ) ) ;
#74225=CARTESIAN_POINT ( 'NONE',  ( 13.74685606122050885, 14.44317598224977672, -1.500000000000002220 ) ) ;
#74226=CARTESIAN_POINT ( 'NONE',  ( -71.62287095715005592, -23.47593901973091235, -1.443836447539006196 ) ) ;
#74228=ORIENTED_EDGE ( 'NONE', *, *, #37654, .F. ) ;
#74229=PLANE ( 'NONE',  #78291 ) ;
#74230=EDGE_CURVE ( 'NONE', #39979, #23609, #43920, .T. ) ;
#74232=CARTESIAN_POINT ( 'NONE',  ( -124.5120777840107138, -25.30063217623697014, 5.394079605411008060 ) ) ;
#74238=B_SPLINE_SURFACE_WITH_KNOTS ( 'NONE', 3, 1, ( 
 ( #42789, #73233 ),
 ( #73720, #64646 ),
 ( #2227, #72233 ),
 ( #2727, #33665 ),
 ( #26044, #57017 ),
 ( #87954, #18435 ),
 ( #49406, #72736 ),
 ( #34170, #65141 ),
 ( #96064, #20412 ),
 ( #6697, #13302 ),
 ( #6200, #21905 ),
 ( #44280, #68114 ),
 ( #53390, #83824 ),
 ( #97552, #75209 ),
 ( #60011, #14303 ),
 ( #5701, #99034 ),
 ( #89943, #51893 ),
 ( #76202, #28052 ),
 ( #35667, #67127 ) ),
 .UNSPECIFIED., .F., .F., .F.,
 ( 4, 1, 1, 1, 1, 1, 1, 1, 1, 1, 1, 1, 1, 1, 1, 1, 4 ),
 ( 2, 2 ),
 ( 0.000000000000000000, 0.06113791491562082375, 0.1199938438512146849, 0.1782253215076174679, 0.2362564202618976927, 0.2949293769549120037, 0.3547157488097547051, 0.4167296639241671041, 0.4806644084708293629, 0.5458317702108683722, 0.6097581054261661526, 0.6729712284742268569, 0.7360168691676639563, 0.7998393981920308704, 0.8647753566655731472, 0.9310876232725697754, 0.9999999999999998890 ),
 ( 0.000000000000000000, 1.000000000000000000 ),
 .UNSPECIFIED. ) ;
#74241=EDGE_LOOP ( 'NONE', ( #93596, #91020, #74149, #48604 ) ) ;
#74242=CARTESIAN_POINT ( 'NONE',  ( 18.08294815051442583, 9.098846914115775064, 11.49999999999998934 ) ) ;
#74243=CARTESIAN_POINT ( 'NONE',  ( -122.5913838597558509, -23.73766607897671221, -1.055555164236450461 ) ) ;
#74244=CARTESIAN_POINT ( 'NONE',  ( -48.62287095715004881, -29.50247984919015209, -1.443849546365058689 ) ) ;
#74245=AXIS2_PLACEMENT_3D ( 'NONE', #16926, #49401, #33660 ) ;
#74246=B_SPLINE_CURVE_WITH_KNOTS ( 'NONE', 3,
 ( #45323, #86865, #64568, #48322 ),
 .UNSPECIFIED., .F., .F.,
 ( 4, 4 ),
 ( 0.9335157282560042624, 0.9630223066614528316 ),
 .UNSPECIFIED. ) ;
#74247=PLANE ( 'NONE',  #2310 ) ;
#74249=CARTESIAN_POINT ( 'NONE',  ( -46.62287095715005592, -24.50321055353805022, 9.387540953477531147 ) ) ;
#74250=FACE_OUTER_BOUND ( 'NONE', #6908, .T. ) ;
#74251=CARTESIAN_POINT ( 'NONE',  ( 19.28819943863484454, -5.468471092112969778, -1.500000000000002220 ) ) ;
#74252=CARTESIAN_POINT ( 'NONE',  ( -10.24336464640716216, -18.35016636821181280, 11.49999999999999645 ) ) ;
#74253=LINE ( 'NONE', #66172, #89112 ) ;
#74255=CARTESIAN_POINT ( 'NONE',  ( -21.55788180805707555, 4.768121097544787190, 11.49999999999998934 ) ) ;
#74258=CARTESIAN_POINT ( 'NONE',  ( -40.38104457131870362, -25.31589329699823665, 5.081426734244629095 ) ) ;
#74259=FACE_OUTER_BOUND ( 'NONE', #65786, .T. ) ;
#74262=CARTESIAN_POINT ( 'NONE',  ( -99.20032484257374961, -25.23532765140830136, 3.605358624617810648 ) ) ;
#74263=CARTESIAN_POINT ( 'NONE',  ( -31.59416852699393985, -24.15543982623907127, -0.2315651400026576545 ) ) ;
#74264=ORIENTED_EDGE ( 'NONE', *, *, #5274, .T. ) ;
#74266=VERTEX_POINT ( 'NONE', #76803 ) ;
#74267=DIRECTION ( 'NONE',  ( 0.000000000000000000, 0.9999999999976377785, 2.173523156925979128E-06 ) ) ;
#74269=CARTESIAN_POINT ( 'NONE',  ( -76.63418747624923810, -24.15543982623907482, -0.2315651400026599305 ) ) ;
#74270=CARTESIAN_POINT ( 'NONE',  ( -4.704028875484805639, -20.06825252194306941, -1.500000000000002220 ) ) ;
#74271=CARTESIAN_POINT ( 'NONE',  ( 19.30674495121141376, 9.566621930910674365, 11.49999999999999645 ) ) ;
#74272=ORIENTED_EDGE ( 'NONE', *, *, #75307, .F. ) ;
#74276=CARTESIAN_POINT ( 'NONE',  ( -97.55620429048337883, -23.48783264082478084, -1.443836473390061936 ) ) ;
#74277=CARTESIAN_POINT ( 'NONE',  ( 19.44376294880228428, 11.01865886811674677, -1.500000000000002220 ) ) ;
#74280=ORIENTED_EDGE ( 'NONE', *, *, #11400, .T. ) ;
#74281=DIRECTION ( 'NONE',  ( 0.000000000000000000, 0.9999999999976377785, 2.173523156925979975E-06 ) ) ;
#74283=VECTOR ( 'NONE', #68000, 1000.000000000000114 ) ;
#74284=CARTESIAN_POINT ( 'NONE',  ( -10.06633388967972209, 18.29571535785830960, -1.500000000000002220 ) ) ;
#74285=EDGE_LOOP ( 'NONE', ( #55613, #75853, #22934, #91904 ) ) ;
#74286=CARTESIAN_POINT ( 'NONE',  ( -86.60313021933721700, -23.48783264082478084, -1.443836473390066155 ) ) ;
#74288=ORIENTED_EDGE ( 'NONE', *, *, #43712, .T. ) ;
#74289=B_SPLINE_CURVE_WITH_KNOTS ( 'NONE', 3,
 ( #77245, #53443, #14854, #6748, #7749, #68662 ),
 .UNSPECIFIED., .F., .F.,
 ( 4, 2, 4 ),
 ( 0.000000000000000000, 0.001380901958385383774, 0.002761803916770767548 ),
 .UNSPECIFIED. ) ;
#74290=CARTESIAN_POINT ( 'NONE',  ( -100.5100443294204808, -24.52399227489127398, 9.353111116836526406 ) ) ;
#74291=CARTESIAN_POINT ( 'NONE',  ( 14.35337761433406811, 15.45585641580067104, -1.500000000000002220 ) ) ;
#74292=ORIENTED_EDGE ( 'NONE', *, *, #86762, .F. ) ;
#74293=CARTESIAN_POINT ( 'NONE',  ( -28.52287095715005094, -23.31182002239687989, -1.443836447538998202 ) ) ;
#74295=CARTESIAN_POINT ( 'NONE',  ( -120.5565306492393916, -23.85049219812686871, 10.88485053497526778 ) ) ;
#74296=CARTESIAN_POINT ( 'NONE',  ( -68.55620429048337883, -23.48786465467241058, 11.44779295918255002 ) ) ;
#74298=CARTESIAN_POINT ( 'NONE',  ( -17.16505717403991227, -13.39166244882208012, -1.500000000000002220 ) ) ;
#74299=CARTESIAN_POINT ( 'NONE',  ( -81.41053730768496166, -25.24759681816308898, 6.535219080203766850 ) ) ;
#74300=EDGE_CURVE ( 'NONE', #477, #76857, #87406, .T. ) ;
#74301=CARTESIAN_POINT ( 'NONE',  ( 11.81759748825469281, -18.92407201980706333, 11.49999999999999645 ) ) ;
#74302=EDGE_LOOP ( 'NONE', ( #25237, #81547, #24319, #54110 ) ) ;
#74305=DIRECTION ( 'NONE',  ( 2.860369681942282691E-39, 2.173523156925979128E-06, -0.9999999999976378895 ) ) ;
#74306=ORIENTED_EDGE ( 'NONE', *, *, #83143, .T. ) ;
#74307=B_SPLINE_CURVE_WITH_KNOTS ( 'NONE', 3,
 ( #29014, #90918, #21386, #52363 ),
 .UNSPECIFIED., .F., .F.,
 ( 4, 4 ),
 ( 0.000000000000000000, 0.0001000000000000028644 ),
 .UNSPECIFIED. ) ;
#74308=CARTESIAN_POINT ( 'NONE',  ( -40.62287095715007013, -23.85196035786900381, -0.8779234886474998056 ) ) ;
#74313=CARTESIAN_POINT ( 'NONE',  ( -128.5228709571500758, -23.47593901973090524, -1.443836447538996204 ) ) ;
#74315=B_SPLINE_CURVE_WITH_KNOTS ( 'NONE', 3,
 ( #92482, #55444, #7754, #1152 ),
 .UNSPECIFIED., .F., .F.,
 ( 4, 4 ),
 ( 0.5508933794777274295, 0.5598998107498430743 ),
 .UNSPECIFIED. ) ;
#74316=CARTESIAN_POINT ( 'NONE',  ( -67.55620429048340725, -23.48786465467240703, 11.44779295918254647 ) ) ;
#74318=CARTESIAN_POINT ( 'NONE',  ( -51.16325253692608754, -25.31574324955554189, 5.002592196407556813 ) ) ;
#74320=CARTESIAN_POINT ( 'NONE',  ( 3.017506814366913481, 19.14668354085002733, 11.49999999999999645 ) ) ;
#74328=PLANE ( 'NONE',  #9911 ) ;
#74329=CARTESIAN_POINT ( 'NONE',  ( -12.94911239430987315, -14.73082512860577609, 11.49999999999998934 ) ) ;
#74330=CARTESIAN_POINT ( 'NONE',  ( -66.55620429048339304, -23.48786465467241058, 11.44779295918255002 ) ) ;
#74332=CARTESIAN_POINT ( 'NONE',  ( -19.93307770644097232, -8.117153041090405807, 11.49999999999998934 ) ) ;
#74333=CARTESIAN_POINT ( 'NONE',  ( -121.5562042904834215, -23.48783264082479505, -1.443836473390058828 ) ) ;
#74334=CARTESIAN_POINT ( 'NONE',  ( -71.26594616156928907, -25.25639464561320935, 6.471657872805320011 ) ) ;
#74335=FACE_OUTER_BOUND ( 'NONE', #77861, .T. ) ;
#74337=CARTESIAN_POINT ( 'NONE',  ( 14.87233727408824713, -17.56007624320114857, -1.500000000000002220 ) ) ;
#74340=CARTESIAN_POINT ( 'NONE',  ( -53.58736094297834285, -24.34968618360933590, 0.1864209137778786440 ) ) ;
#74341=CARTESIAN_POINT ( 'NONE',  ( 19.08902475966321788, 6.433202353099247262, 11.49999999999999645 ) ) ;
#74342=CARTESIAN_POINT ( 'NONE',  ( -45.62287095715004881, -23.47596703998600276, 11.44779298504227505 ) ) ;
#74347=CARTESIAN_POINT ( 'NONE',  ( -126.5562042904833646, -23.48786465467241769, 11.44779295918253581 ) ) ;
#74348=CARTESIAN_POINT ( 'NONE',  ( -19.77004505525285083, 2.005399880840008642, 11.49999999999998934 ) ) ;
#74350=CARTESIAN_POINT ( 'NONE',  ( 16.89532177248590372, -10.13005384644002227, -1.500000000000002220 ) ) ;
#74353=CARTESIAN_POINT ( 'NONE',  ( -111.5228709571500616, -24.65952944569305316, 1.056160979905704123 ) ) ;
#74354=CARTESIAN_POINT ( 'NONE',  ( -13.08992234710881064, 15.94516925376868244, 11.49999999999999645 ) ) ;
#74355=CARTESIAN_POINT ( 'NONE',  ( -75.62287095715005592, -23.47596703998600631, 11.44779298504227860 ) ) ;
#74358=CARTESIAN_POINT ( 'NONE',  ( 3.867644355387967359, 22.30990608135428488, 11.49999999999999645 ) ) ;
#74359=EDGE_CURVE ( 'NONE', #26538, #95555, #96053, .T. ) ;
#74360=ORIENTED_EDGE ( 'NONE', *, *, #58901, .T. ) ;
#74361=CARTESIAN_POINT ( 'NONE',  ( -25.53098197642538736, -24.92569209777881056, 4.942811685741776984 ) ) ;
#74363=CARTESIAN_POINT ( 'NONE',  ( -63.58341162693596971, -24.51314013834316796, 0.6176544820404160641 ) ) ;
#74364=DIRECTION ( 'NONE',  ( 0.000000000000000000, -2.173523156925979975E-06, 0.9999999999976378895 ) ) ;
#74365=ORIENTED_EDGE ( 'NONE', *, *, #44669, .F. ) ;
#74366=ORIENTED_EDGE ( 'NONE', *, *, #28287, .F. ) ;
#74368=CARTESIAN_POINT ( 'NONE',  ( 22.56601425305882813, -3.627385684441148506, 11.49999999999998934 ) ) ;
#74369=CARTESIAN_POINT ( 'NONE',  ( -29.56144451721570832, -23.65455177597154091, -1.055554856561816246 ) ) ;
#74370=B_SPLINE_CURVE_WITH_KNOTS ( 'NONE', 3,
 ( #69158, #76748, #43477, #4908, #30594, #28238, #31090, #69668 ),
 .UNSPECIFIED., .F., .F.,
 ( 4, 2, 2, 4 ),
 ( -0.001240666984355830215, -0.0002401179793394881724, 0.0007604310256768538698, 0.002761529035709538171 ),
 .UNSPECIFIED. ) ;
#74371=CARTESIAN_POINT ( 'NONE',  ( 5.819084965910729323, 20.79142713412266730, -1.500000000000002220 ) ) ;
#74372=CARTESIAN_POINT ( 'NONE',  ( -113.6235176254694750, -24.66019654487200086, 8.947790411086106843 ) ) ;
#74373=DIRECTION ( 'NONE',  ( 0.000000000000000000, -2.173523156925979552E-06, 0.9999999999976378895 ) ) ;
#74374=CARTESIAN_POINT ( 'NONE',  ( 21.16815136333514502, -7.790938087775149512, 11.49999999999999645 ) ) ;
#74376=CARTESIAN_POINT ( 'NONE',  ( -69.64187497903644442, -25.31612452842404437, 5.000677404731540321 ) ) ;
#74377=CARTESIAN_POINT ( 'NONE',  ( 21.66556372666567754, 3.824538051775513647, -1.500000000000002220 ) ) ;
#74378=EDGE_CURVE ( 'NONE', #81873, #95644, #16049, .T. ) ;
#74379=CARTESIAN_POINT ( 'NONE',  ( -111.5570160696827173, -23.73766607897670511, -1.055555164236450461 ) ) ;
#74383=CARTESIAN_POINT ( 'NONE',  ( -107.5228709571500758, -24.64965694238575011, 8.947790433994192938 ) ) ;
#74384=EDGE_LOOP ( 'NONE', ( #99028, #27448, #87033, #79491 ) ) ;
#74385=CARTESIAN_POINT ( 'NONE',  ( -84.62287095715005592, -24.64898659630367561, 1.056161002820826145 ) ) ;
#74390=ORIENTED_EDGE ( 'NONE', *, *, #68768, .F. ) ;
#74391=DIRECTION ( 'NONE',  ( -3.773278334453080206E-23, 0.9999999999976377785, 2.173523156925979975E-06 ) ) ;
#74392=DIRECTION ( 'NONE',  ( -3.773278334453079030E-23, 0.9999999999976377785, 2.173523156925979128E-06 ) ) ;
#74393=CARTESIAN_POINT ( 'NONE',  ( -115.6228709571500417, -25.00182538069145721, 7.747789668545097541 ) ) ;
#74394=CARTESIAN_POINT ( 'NONE',  ( -19.95082702767638239, -4.354873812894156870, -1.500000000000002220 ) ) ;
#74396=CARTESIAN_POINT ( 'NONE',  ( -71.03488587359156270, -25.06952888890338471, 7.387088048512346461 ) ) ;
#74400=ADVANCED_FACE ( 'NONE', ( #57510 ), #49395, .T. ) ;
#74401=CARTESIAN_POINT ( 'NONE',  ( -105.5906832248129490, -24.40034930558991277, 0.3402023900116059041 ) ) ;
#74402=CARTESIAN_POINT ( 'NONE',  ( -70.52593452554701514, -25.03149848527395704, 7.557317387464395075 ) ) ;
#74403=EDGE_LOOP ( 'NONE', ( #4417, #51681, #96400, #25064 ) ) ;
#74404=CARTESIAN_POINT ( 'NONE',  ( -122.6228709571500417, -23.47593901973091235, -1.443836447538997536 ) ) ;
#74405=CARTESIAN_POINT ( 'NONE',  ( -88.22287095715005023, -23.47593901973090169, -1.443836447538996870 ) ) ;
#74406=ADVANCED_FACE ( 'NONE', ( #64130 ), #95049, .T. ) ;
#74408=VECTOR ( 'NONE', #592, 1000.000000000000114 ) ;
#74409=CARTESIAN_POINT ( 'NONE',  ( 19.72710162658169608, 6.580912942549038469, 11.49999999999998934 ) ) ;
#74411=CARTESIAN_POINT ( 'NONE',  ( -39.56951972374358206, -25.30125091222718225, 4.659097539256057630 ) ) ;
#74412=ORIENTED_EDGE ( 'NONE', *, *, #60112, .F. ) ;
#74413=CARTESIAN_POINT ( 'NONE',  ( -51.52764846858840997, -25.12217663958179870, 6.187573060801323521 ) ) ;
#74414=PLANE ( 'NONE',  #37317 ) ;
#74415=ORIENTED_EDGE ( 'NONE', *, *, #29261, .T. ) ;
#74416=ORIENTED_EDGE ( 'NONE', *, *, #40680, .F. ) ;
#74417=CARTESIAN_POINT ( 'NONE',  ( -112.6228709571500701, -23.48783264082479150, -1.443836473390060160 ) ) ;
#74419=CARTESIAN_POINT ( 'NONE',  ( -118.3656746162385645, -25.21753786267797892, 3.540021004441392893 ) ) ;
#74421=B_SPLINE_CURVE_WITH_KNOTS ( 'NONE', 3,
 ( #40916, #26696, #88102, #19070 ),
 .UNSPECIFIED., .F., .F.,
 ( 4, 4 ),
 ( 0.000000000000000000, 9.999999999997510880E-05 ),
 .UNSPECIFIED. ) ;
#74422=CARTESIAN_POINT ( 'NONE',  ( -43.60020624437694181, -23.96169478059712432, 10.65365249895718769 ) ) ;
#74424=CARTESIAN_POINT ( 'NONE',  ( -21.77411086464670831, -3.637377321037103872, 11.49999999999999645 ) ) ;
#74425=ORIENTED_EDGE ( 'NONE', *, *, #41191, .F. ) ;
#74426=CARTESIAN_POINT ( 'NONE',  ( -72.62287095715005592, -23.48783264082478084, -1.443836473390067265 ) ) ;
#74427=CARTESIAN_POINT ( 'NONE',  ( 22.24477432615492134, 4.004077059304647968, 11.49999999999998934 ) ) ;
#74428=FACE_OUTER_BOUND ( 'NONE', #76552, .T. ) ;
#74429=ORIENTED_EDGE ( 'NONE', *, *, #12202, .T. ) ;
#74430=ORIENTED_EDGE ( 'NONE', *, *, #1362, .T. ) ;
#74433=EDGE_CURVE ( 'NONE', #15452, #49598, #19421, .T. ) ;
#74434=B_SPLINE_SURFACE_WITH_KNOTS ( 'NONE', 3, 1, ( 
 ( #62154, #63154 ),
 ( #8849, #45928 ),
 ( #76350, #23561 ),
 ( #53045, #92576 ),
 ( #53544, #39797 ),
 ( #99678, #70755 ),
 ( #83975, #68758 ),
 ( #736, #30181 ),
 ( #30686, #76839 ),
 ( #8348, #54044 ),
 ( #69252, #54531 ),
 ( #23054, #7847 ),
 ( #7341, #22553 ),
 ( #31689, #238 ),
 ( #55037, #100170 ),
 ( #84969, #77347 ),
 ( #38796, #15951 ),
 ( #70253, #93572 ),
 ( #41822, #18462 ) ),
 .UNSPECIFIED., .F., .F., .F.,
 ( 4, 1, 1, 1, 1, 1, 1, 1, 1, 1, 1, 1, 1, 1, 1, 1, 4 ),
 ( 2, 2 ),
 ( 0.000000000000000000, 0.07524330859112852987, 0.1472088117202518809, 0.2164470898547687372, 0.2840250416193483840, 0.3506554491966432097, 0.4150313178410243720, 0.4796298309645117830, 0.5446516341371376857, 0.6080442396977419062, 0.6678275650288183485, 0.7251142466493384342, 0.7809917079106386550, 0.8355270040618592020, 0.8894381545415823709, 0.9440720891799450065, 1.000000000000000000 ),
 ( 0.000000000000000000, 1.000000000000000000 ),
 .UNSPECIFIED. ) ;
#74435=CARTESIAN_POINT ( 'NONE',  ( -57.55355702163512177, -23.96169478059713143, 10.65365249895718058 ) ) ;
#74436=ORIENTED_EDGE ( 'NONE', *, *, #19534, .F. ) ;
#74438=CARTESIAN_POINT ( 'NONE',  ( 1.165341552704713513, 22.26021350444069213, -1.500000000000002220 ) ) ;
#74439=DIRECTION ( 'NONE',  ( -1.000000000000000000, -3.773278334444167608E-23, -8.201307810031802745E-29 ) ) ;
#74440=EDGE_CURVE ( 'NONE', #54707, #61052, #72724, .T. ) ;
#74441=EDGE_LOOP ( 'NONE', ( #20247, #2764, #79301, #96058 ) ) ;
#74444=ADVANCED_FACE ( 'NONE', ( #48383 ), #3227, .F. ) ;
#74445=CARTESIAN_POINT ( 'NONE',  ( -70.52287095715007581, -23.47593901973090524, -1.443836447538997092 ) ) ;
#74448=CARTESIAN_POINT ( 'NONE',  ( -18.91883139384513157, -4.797682538509264738, -1.500000000000002220 ) ) ;
#74449=CARTESIAN_POINT ( 'NONE',  ( 20.36625868517733196, 6.724766957447481097, -1.500000000000002220 ) ) ;
#74451=CARTESIAN_POINT ( 'NONE',  ( -41.52287095715006870, -29.50247984919015209, -1.443849546365060466 ) ) ;
#74452=CARTESIAN_POINT ( 'NONE',  ( -48.52287095715006160, -23.47596703998600631, 11.44779298504229104 ) ) ;
#74453=CARTESIAN_POINT ( 'NONE',  ( -12.44792101662413408, -19.12764231104124946, -1.500000000000002220 ) ) ;
#74455=CARTESIAN_POINT ( 'NONE',  ( -49.50841769935765768, -25.27292115247390569, 3.984447733149576898 ) ) ;
#74456=CARTESIAN_POINT ( 'NONE',  ( -50.52287095715006160, -23.48786465467241058, 11.44779295918255002 ) ) ;
#74457=CARTESIAN_POINT ( 'NONE',  ( 6.038693664686949347, 19.05185810397003721, 11.49999999999999645 ) ) ;
#74458=CARTESIAN_POINT ( 'NONE',  ( -101.6228709571500559, -24.66019654487199730, 8.947790411086121054 ) ) ;
#74460=CARTESIAN_POINT ( 'NONE',  ( -74.51666087527418370, -23.73791477778911840, 11.05961554403170588 ) ) ;
#74461=PLANE ( 'NONE',  #29391 ) ;
#74463=CARTESIAN_POINT ( 'NONE',  ( -26.02075258637046673, -24.72833475862651653, 2.618636308606199226 ) ) ;
#74464=CARTESIAN_POINT ( 'NONE',  ( -124.5228709571501611, -24.34917612406838572, 0.1852690917426621509 ) ) ;
#74465=CARTESIAN_POINT ( 'NONE',  ( 19.97611268498323511, -8.487024919450899318, 11.49999999999998934 ) ) ;
#74468=CARTESIAN_POINT ( 'NONE',  ( -19.43040671759091609, -1.856541507571394467, -1.500000000000002220 ) ) ;
#74469=CARTESIAN_POINT ( 'NONE',  ( -100.3031470170733712, -25.13382359911133435, 7.097745423514688845 ) ) ;
#74471=ORIENTED_EDGE ( 'NONE', *, *, #68896, .F. ) ;
#74474=CARTESIAN_POINT ( 'NONE',  ( 14.46511082492616573, -14.46070965572739730, 11.49999999999999645 ) ) ;
#74476=CARTESIAN_POINT ( 'NONE',  ( -39.62287095715005592, -24.64965695001468404, 8.947790433994187609 ) ) ;
#74478=VERTEX_POINT ( 'NONE', #34161 ) ;
#74480=DIRECTION ( 'NONE',  ( -3.773278334453079618E-23, 0.9999999999976377785, 2.173523156925979975E-06 ) ) ;
#74481=CARTESIAN_POINT ( 'NONE',  ( -78.62287095715005592, -23.47593901973091235, -1.443836447539004642 ) ) ;
#74482=B_SPLINE_CURVE_WITH_KNOTS ( 'NONE', 3,
 ( #29507, #14277, #3825, #60487 ),
 .UNSPECIFIED., .F., .F.,
 ( 4, 4 ),
 ( 0.000000000000000000, 9.999999999998897304E-05 ),
 .UNSPECIFIED. ) ;
#74483=CARTESIAN_POINT ( 'NONE',  ( -85.52287095715006160, -23.85196035786899316, -0.8779234886475173472 ) ) ;
#74485=CARTESIAN_POINT ( 'NONE',  ( -80.34687923781922336, -25.14083923594767356, 2.947789366383932297 ) ) ;
#74486=CARTESIAN_POINT ( 'NONE',  ( 22.64363655503811046, -4.068770074275382953, 11.49999999999999645 ) ) ;
#74487=CARTESIAN_POINT ( 'NONE',  ( -22.52399778787742335, 3.408274809117095572, -1.500000000000002220 ) ) ;
#74488=CARTESIAN_POINT ( 'NONE',  ( -110.5527773381347458, -24.40133493613049609, 9.663955038902800609 ) ) ;
#74489=CARTESIAN_POINT ( 'NONE',  ( -40.52287095715006160, -23.84047902841603417, -0.8780736468305391229 ) ) ;
#74490=CARTESIAN_POINT ( 'NONE',  ( -98.89303308397303738, -25.25494757631710385, 6.110950176066591411 ) ) ;
#74491=CARTESIAN_POINT ( 'NONE',  ( -70.52287095715007581, -25.00158670708909625, 2.256160236439166411 ) ) ;
#74492=CARTESIAN_POINT ( 'NONE',  ( -110.5886823328070534, -24.63355581998384380, 0.9682620441943931011 ) ) ;
#74493=CARTESIAN_POINT ( 'NONE',  ( 19.94191871449930531, -9.063712221575384476, -1.500000000000002220 ) ) ;
#74494=CARTESIAN_POINT ( 'NONE',  ( -59.58953762381670316, -24.64965694238406968, 8.947790433994660120 ) ) ;
#74495=EDGE_CURVE ( 'NONE', #26773, #36250, #64437, .T. ) ;
#74496=CARTESIAN_POINT ( 'NONE',  ( -50.58953762381672448, -23.48786465467241058, 11.44779295918255180 ) ) ;
#74497=CARTESIAN_POINT ( 'NONE',  ( -120.6228709571500985, -24.62226745350444190, 0.9660975649729637293 ) ) ;
#74498=CARTESIAN_POINT ( 'NONE',  ( -96.52287095715006160, -24.50321055353804311, 9.387540953477515160 ) ) ;
#74500=CARTESIAN_POINT ( 'NONE',  ( 13.86372479123709311, 15.02075200336711092, 11.49999999999998934 ) ) ;
#74505=CARTESIAN_POINT ( 'NONE',  ( 15.83906049732654608, 16.74391201645830662, -1.500000000000002220 ) ) ;
#74506=CARTESIAN_POINT ( 'NONE',  ( -57.62287095715004881, -29.50250243563736774, 8.947779886222145151 ) ) ;
#74507=CARTESIAN_POINT ( 'NONE',  ( 0.8729654516333695824, -20.24016528753796962, -1.500000000000002220 ) ) ;
#74509=EDGE_CURVE ( 'NONE', #82785, #30829, #56007, .T. ) ;
#74510=CARTESIAN_POINT ( 'NONE',  ( -93.62287095715005592, -29.50250243563736774, 8.947779886222139822 ) ) ;
#74511=ADVANCED_FACE ( 'NONE', ( #6688 ), #45263, .T. ) ;
#74512=CARTESIAN_POINT ( 'NONE',  ( -48.52287095715006870, -24.51387760970724372, 9.387446482453402297 ) ) ;
#74513=EDGE_CURVE ( 'NONE', #6511, #72410, #6351, .T. ) ;
#74514=CARTESIAN_POINT ( 'NONE',  ( -51.62287095715007013, -24.33927499327855415, 9.819080762295820719 ) ) ;
#74515=CARTESIAN_POINT ( 'NONE',  ( -41.62287095715006302, -23.47596703998600276, 11.44779298504227505 ) ) ;
#74516=CARTESIAN_POINT ( 'NONE',  ( 9.194277187580093269, -19.27880637823015419, 11.49999999999999645 ) ) ;
#74517=EDGE_LOOP ( 'NONE', ( #41458, #16381, #16507, #26740 ) ) ;
#74518=CARTESIAN_POINT ( 'NONE',  ( -55.52287095715005449, -23.84047902841601996, -0.8780736468305719855 ) ) ;
#74519=EDGE_CURVE ( 'NONE', #90247, #3242, #20400, .T. ) ;
#74520=ORIENTED_EDGE ( 'NONE', *, *, #47746, .F. ) ;
#74521=CARTESIAN_POINT ( 'NONE',  ( 15.88595335714125589, -15.59144682577495189, -1.500000000000002220 ) ) ;
#74522=B_SPLINE_CURVE_WITH_KNOTS ( 'NONE', 3,
 ( #87475, #17967, #40305, #78842 ),
 .UNSPECIFIED., .F., .F.,
 ( 4, 4 ),
 ( 0.000000000000000000, 1.000000000000000000 ),
 .UNSPECIFIED. ) ;
#74523=CARTESIAN_POINT ( 'NONE',  ( -4.528870947376731237, 20.18191347215651987, 11.49999999999998934 ) ) ;
#74526=CARTESIAN_POINT ( 'NONE',  ( -28.57383953491463657, -24.50287364620303521, 1.056161677404372501 ) ) ;
#74527=EDGE_LOOP ( 'NONE', ( #96488, #97771, #73702, #7990 ) ) ;
#74531=CARTESIAN_POINT ( 'NONE',  ( -17.10473743203234775, -12.04273770408705246, -1.500000000000002220 ) ) ;
#74533=CARTESIAN_POINT ( 'NONE',  ( -0.1377007522546883911, -21.91379463844567965, 11.49999999999999645 ) ) ;
#74534=CARTESIAN_POINT ( 'NONE',  ( -37.63489630462677127, -24.35071581493542325, 9.817618358456030592 ) ) ;
#74535=CARTESIAN_POINT ( 'NONE',  ( 12.90280524143238594, -18.44629484376132922, -1.500000000000002220 ) ) ;
#74537=CARTESIAN_POINT ( 'NONE',  ( 17.09260067683297635, -12.12037977771017871, -1.500000000000002220 ) ) ;
#74538=DIRECTION ( 'NONE',  ( 0.000000000000000000, -0.9999999999976377785, -2.173523156925979975E-06 ) ) ;
#74539=CARTESIAN_POINT ( 'NONE',  ( -81.62287095715004170, -23.48786465467241058, 11.44779295918254647 ) ) ;
#74543=AXIS2_PLACEMENT_3D ( 'NONE', #4529, #35478, #41595 ) ;
#74544=ORIENTED_EDGE ( 'NONE', *, *, #6475, .T. ) ;
#74548=ADVANCED_FACE ( 'NONE', ( #91416 ), #59488, .T. ) ;
#74550=CARTESIAN_POINT ( 'NONE',  ( 11.86944616785735818, -17.87650476368427732, -1.500000000000002220 ) ) ;
#74552=ORIENTED_EDGE ( 'NONE', *, *, #85735, .F. ) ;
#74553=CARTESIAN_POINT ( 'NONE',  ( -3.607955376466517095, 20.77440192976073519, 11.49999999999998934 ) ) ;
#74554=CARTESIAN_POINT ( 'NONE',  ( -100.3262102087699787, -25.19537855052032782, 3.296406834188733370 ) ) ;
#74559=CARTESIAN_POINT ( 'NONE',  ( -22.05048665130746954, -1.834114841651104832, -1.500000000000002220 ) ) ;
#74560=CARTESIAN_POINT ( 'NONE',  ( -81.54104209881381848, -24.66019654487198665, 8.947790411086131712 ) ) ;
#74561=CARTESIAN_POINT ( 'NONE',  ( -109.8650282762807393, -25.28040082146351608, 5.784628005357986602 ) ) ;
#74564=CARTESIAN_POINT ( 'NONE',  ( -100.5937343098658943, -24.15503026093918137, -0.2815557561904373229 ) ) ;
#74565=CARTESIAN_POINT ( 'NONE',  ( 4.555389213293416617, -20.86945110937667280, -1.500000000000002220 ) ) ;
#74566=CARTESIAN_POINT ( 'NONE',  ( -26.16584078008908421, -24.94396127023346210, 5.878266566680999894 ) ) ;
#74567=CARTESIAN_POINT ( 'NONE',  ( -51.95662050938321386, -25.03707831087709579, 7.590867751134624974 ) ) ;
#74570=CARTESIAN_POINT ( 'NONE',  ( -70.34217583644009153, -25.29972316739413429, 4.286145325355288804 ) ) ;
#74571=CARTESIAN_POINT ( 'NONE',  ( 20.84710439121840864, 8.857176948214046774, -1.500000000000002220 ) ) ;
#74575=CARTESIAN_POINT ( 'NONE',  ( 8.221391366598689743, 17.94232518691122635, 11.49999999999999645 ) ) ;
#74577=CARTESIAN_POINT ( 'NONE',  ( -119.5228709571500758, -24.65952944569305316, 1.056160979905705899 ) ) ;
#74578=EDGE_LOOP ( 'NONE', ( #25466, #15735, #68909, #72908 ) ) ;
#74580=CARTESIAN_POINT ( 'NONE',  ( -28.79528301136424417, -24.60093966666663690, 1.979581142082611489 ) ) ;
#74581=CARTESIAN_POINT ( 'NONE',  ( -75.52287095715007581, -24.52323809116984776, 9.355190652339432589 ) ) ;
#74582=CARTESIAN_POINT ( 'NONE',  ( -16.79864850723062020, -13.61054813162024679, 11.49999999999998934 ) ) ;
#74583=CARTESIAN_POINT ( 'NONE',  ( -49.11088876609831289, -25.27518098729074225, 3.850711683794803886 ) ) ;
#74584=CARTESIAN_POINT ( 'NONE',  ( 4.481524277812761525, 18.85844072219565604, -1.500000000000002220 ) ) ;
#74586=CARTESIAN_POINT ( 'NONE',  ( -80.85468212908030239, -25.05082048915169679, 7.526967310880902318 ) ) ;
#74587=CARTESIAN_POINT ( 'NONE',  ( 18.24360591643979035, -7.691401616277519615, 11.49999999999998934 ) ) ;
#74589=CARTESIAN_POINT ( 'NONE',  ( -13.42616926349082895, -15.17935092467416069, 11.49999999999999645 ) ) ;
#74592=B_SPLINE_CURVE_WITH_KNOTS ( 'NONE', 3,
 ( #56474, #70174, #54455, #16884, #31606, #23474, #55969, #71686 ),
 .UNSPECIFIED., .F., .F.,
 ( 4, 2, 2, 4 ),
 ( -0.001240355328176780516, -0.0002398155169398910602, 0.0007607242942969983952, 0.002761803916770777523 ),
 .UNSPECIFIED. ) ;
#74595=CARTESIAN_POINT ( 'NONE',  ( -99.52764846858842418, -25.26416398485831749, 3.999772271414141489 ) ) ;
#74597=CARTESIAN_POINT ( 'NONE',  ( -44.62287095715005592, -24.51283580621362646, 0.6167428607019806996 ) ) ;
#74598=CARTESIAN_POINT ( 'NONE',  ( -95.62287095715005592, -23.48783264082479150, -1.443836473390061936 ) ) ;
#74599=CARTESIAN_POINT ( 'NONE',  ( -31.52287095715006870, -23.72773821059535848, 11.05748984161097503 ) ) ;
#74600=CARTESIAN_POINT ( 'NONE',  ( 3.179702300980958185, 19.78100630842630281, 11.49999999999998934 ) ) ;
#74602=EDGE_LOOP ( 'NONE', ( #65718, #60439, #97225, #8380 ) ) ;
#74606=CARTESIAN_POINT ( 'NONE',  ( -51.52287095715006870, -24.64898659630367206, 1.056161002820821038 ) ) ;
#74607=VECTOR ( 'NONE', #52156, 1000.000000000000114 ) ;
#74612=ORIENTED_EDGE ( 'NONE', *, *, #75245, .F. ) ;
#74614=CARTESIAN_POINT ( 'NONE',  ( 13.61570878652767291, 15.11107311891478666, 11.49999999999998934 ) ) ;
#74615=ORIENTED_EDGE ( 'NONE', *, *, #87184, .T. ) ;
#74617=CARTESIAN_POINT ( 'NONE',  ( 15.56936346670522120, 16.85858822313069894, 11.49999999999998934 ) ) ;
#74618=DIRECTION ( 'NONE',  ( 0.000000000000000000, -0.9999999999976377785, -2.173523156925979128E-06 ) ) ;
#74619=EDGE_CURVE ( 'NONE', #10895, #234, #75690, .T. ) ;
#74620=ORIENTED_EDGE ( 'NONE', *, *, #37587, .T. ) ;
#74621=CARTESIAN_POINT ( 'NONE',  ( -42.62287095715004881, -23.48786465467240347, 11.44779295918255180 ) ) ;
#74623=CARTESIAN_POINT ( 'NONE',  ( -49.58282627629191808, -25.12215357654226011, 6.816471934855654169 ) ) ;
#74624=CARTESIAN_POINT ( 'NONE',  ( -90.52287095715006160, -29.50249982740957577, 7.747779886224967605 ) ) ;
#74625=CARTESIAN_POINT ( 'NONE',  ( -20.82729772986975547, -4.079710536234080642, 11.49999999999999645 ) ) ;
#74627=ORIENTED_EDGE ( 'NONE', *, *, #14238, .F. ) ;
#74628=CARTESIAN_POINT ( 'NONE',  ( -21.91774099701738621, 3.392077650570975766, -1.500000000000002220 ) ) ;
#74629=CARTESIAN_POINT ( 'NONE',  ( 7.647619880454145758, 19.11525441646967849, -1.500000000000002220 ) ) ;
#74631=ORIENTED_EDGE ( 'NONE', *, *, #2836, .T. ) ;
#74634=PLANE ( 'NONE',  #6 ) ;
#74635=ORIENTED_EDGE ( 'NONE', *, *, #20672, .T. ) ;
#74637=ORIENTED_EDGE ( 'NONE', *, *, #79580, .F. ) ;
#74638=CARTESIAN_POINT ( 'NONE',  ( -83.62287095715002749, -24.51283580621364777, 0.6167428607019832532 ) ) ;
#74641=CARTESIAN_POINT ( 'NONE',  ( 20.74337371777590278, 0.4424840333690017724, -1.500000000000002220 ) ) ;
#74642=CARTESIAN_POINT ( 'NONE',  ( -21.72135255055207281, 0.4632500610043824851, 11.49999999999999645 ) ) ;
#74644=CARTESIAN_POINT ( 'NONE',  ( -39.45263493068827643, -25.26937817949567133, 4.062928063294833692 ) ) ;
#74645=CARTESIAN_POINT ( 'NONE',  ( -34.58953762381673869, -23.47596703998600276, 11.44779298504227505 ) ) ;
#74646=CARTESIAN_POINT ( 'NONE',  ( -82.52287095715006160, -23.48786465467241058, 11.44779295918254469 ) ) ;
#74647=CARTESIAN_POINT ( 'NONE',  ( -3.561414601982806349, 22.15502443119318343, -1.500000000000002220 ) ) ;
#74648=CARTESIAN_POINT ( 'NONE',  ( -50.88361436997121245, -25.31296737229286009, 4.608108779064076899 ) ) ;
#74649=CARTESIAN_POINT ( 'NONE',  ( -65.53968771207756561, -24.63355581998386867, 0.9682620441943842193 ) ) ;
#74650=ORIENTED_EDGE ( 'NONE', *, *, #51601, .T. ) ;
#74651=CARTESIAN_POINT ( 'NONE',  ( -98.52287095715006160, -24.50321055353803956, 9.387540953477515160 ) ) ;
#74654=ORIENTED_EDGE ( 'NONE', *, *, #93858, .F. ) ;
#74655=AXIS2_PLACEMENT_3D ( 'NONE', #79774, #9767, #41739 ) ;
#74656=CARTESIAN_POINT ( 'NONE',  ( -46.56050914129246365, -23.73791477778911840, 11.05961554403171299 ) ) ;
#74657=ORIENTED_EDGE ( 'NONE', *, *, #2261, .T. ) ;
#74658=CARTESIAN_POINT ( 'NONE',  ( 11.00477826368897283, 18.22718707545001138, -1.500000000000002220 ) ) ;
#74659=B_SPLINE_CURVE_WITH_KNOTS ( 'NONE', 3,
 ( #40390, #85048, #1832, #7927, #17040, #55118 ),
 .UNSPECIFIED., .F., .F.,
 ( 4, 2, 4 ),
 ( 6.384118678608765745E-06, 0.001386860460828371082, 0.002767336802978133652 ),
 .UNSPECIFIED. ) ;
#74662=CARTESIAN_POINT ( 'NONE',  ( 21.44370820036873937, 4.193779532373530294, -1.500000000000002220 ) ) ;
#74663=CARTESIAN_POINT ( 'NONE',  ( -32.62287095715004881, -29.50248528299804818, 1.056150453629029817 ) ) ;
#74664=CARTESIAN_POINT ( 'NONE',  ( -7.973561950239375307, 21.24132968703115765, -1.500000000000002220 ) ) ;
#74667=CARTESIAN_POINT ( 'NONE',  ( -16.46405638241306946, -14.47283864684382237, -1.500000000000002220 ) ) ;
#74668=CARTESIAN_POINT ( 'NONE',  ( -87.50770710757781501, -24.34968618360934656, 0.1864209137778970737 ) ) ;
#74669=ORIENTED_EDGE ( 'NONE', *, *, #40250, .T. ) ;
#74670=CARTESIAN_POINT ( 'NONE',  ( -40.13634460731591957, -25.29441190524739369, 5.523624973409209993 ) ) ;
#74673=EDGE_CURVE ( 'NONE', #11637, #56992, #29521, .T. ) ;
#74674=CARTESIAN_POINT ( 'NONE',  ( -84.62911920018937906, -24.35071581493543391, 9.817618358456027039 ) ) ;
#74675=AXIS2_PLACEMENT_3D ( 'NONE', #8298, #6792, #45869 ) ;
#74676=CARTESIAN_POINT ( 'NONE',  ( -130.5728709571500303, -24.75179208683297816, 8.640809912072070276 ) ) ;
#74678=CARTESIAN_POINT ( 'NONE',  ( -20.46794915382770341, -22.99521002796696934, -0.9709657327914291702 ) ) ;
#74679=CARTESIAN_POINT ( 'NONE',  ( 9.380127297304197143, -19.07726845333505494, 11.49999999999998934 ) ) ;
#74680=CARTESIAN_POINT ( 'NONE',  ( -55.62287095715007723, -24.52323809116985487, 9.355190652339427260 ) ) ;
#74681=CARTESIAN_POINT ( 'NONE',  ( -26.55847933594999333, -24.97064538767926933, 2.904079897768723661 ) ) ;
#74682=EDGE_CURVE ( 'NONE', #7353, #14136, #35657, .T. ) ;
#74683=CARTESIAN_POINT ( 'NONE',  ( -85.54663212275447393, -24.52300882791530157, 0.6510814631126307095 ) ) ;
#74684=LINE ( 'NONE', #82795, #28126 ) ;
#74685=CARTESIAN_POINT ( 'NONE',  ( -117.5566936961534310, -23.73791477778912551, 11.05961554403169878 ) ) ;
#74686=EDGE_LOOP ( 'NONE', ( #10849, #82142, #59174, #42409 ) ) ;
#74687=CARTESIAN_POINT ( 'NONE',  ( -4.924063254364682507, -18.92933890202812464, 11.49999999999999645 ) ) ;
#74688=CARTESIAN_POINT ( 'NONE',  ( -78.52287095715006160, -24.51387760970723662, 9.387446482453398744 ) ) ;
#74689=CARTESIAN_POINT ( 'NONE',  ( -73.62287095715005592, -29.50247984919015209, -1.443849546365055359 ) ) ;
#74690=ORIENTED_EDGE ( 'NONE', *, *, #94246, .T. ) ;
#74692=CARTESIAN_POINT ( 'NONE',  ( -44.52287095715006160, -24.65952944569303895, 1.056160979905691910 ) ) ;
#74693=CARTESIAN_POINT ( 'NONE',  ( -26.49999761102944618, -24.66668825682660326, 7.831587328706810958 ) ) ;
#74694=CARTESIAN_POINT ( 'NONE',  ( -106.5228709571500332, -24.51283580621365843, 0.6167428607019763698 ) ) ;
#74695=CARTESIAN_POINT ( 'NONE',  ( 11.96684523812195700, 15.63349346248531546, -1.500000000000002220 ) ) ;
#74696=ORIENTED_EDGE ( 'NONE', *, *, #13406, .F. ) ;
#74697=DIRECTION ( 'NONE',  ( -3.773278334453079030E-23, 0.9999999999976377785, 2.173523156925979128E-06 ) ) ;
#74700=ORIENTED_EDGE ( 'NONE', *, *, #3614, .T. ) ;
#74703=CARTESIAN_POINT ( 'NONE',  ( -47.49417500838666939, -24.34968618360933590, 0.1864209137778879144 ) ) ;
#74704=CARTESIAN_POINT ( 'NONE',  ( -118.5578086755916871, -23.48783264082477018, -1.443836473390085695 ) ) ;
#74707=CARTESIAN_POINT ( 'NONE',  ( -107.5534875950873186, -24.15543982623908192, -0.2315651400026443874 ) ) ;
#74708=CARTESIAN_POINT ( 'NONE',  ( 0.05828707793547563409, -19.95834144014285272, -1.500000000000002220 ) ) ;
#74710=CARTESIAN_POINT ( 'NONE',  ( -0.05362039087632652912, -22.35584190302588681, 9.068352157775928291 ) ) ;
#74711=VERTEX_POINT ( 'NONE', #59000 ) ;
#74714=B_SPLINE_CURVE_WITH_KNOTS ( 'NONE', 3,
 ( #89360, #12219, #19828, #5617 ),
 .UNSPECIFIED., .F., .F.,
 ( 4, 4 ),
 ( 0.000000000000000000, 1.000000000000000000 ),
 .UNSPECIFIED. ) ;
#74716=CARTESIAN_POINT ( 'NONE',  ( -80.63529280476316785, -24.40133493613050319, 9.663955038902802386 ) ) ;
#74717=CARTESIAN_POINT ( 'NONE',  ( -125.2170126610060947, -25.23515688875662732, 6.311387300439234238 ) ) ;
#74718=CARTESIAN_POINT ( 'NONE',  ( -81.59562872226922536, -23.96119346886881019, -0.6495511937831893734 ) ) ;
#74720=DIRECTION ( 'NONE',  ( -3.773278334453079030E-23, 0.9999999999976377785, 2.173523156925979128E-06 ) ) ;
#74722=ORIENTED_EDGE ( 'NONE', *, *, #93866, .F. ) ;
#74723=CARTESIAN_POINT ( 'NONE',  ( -37.62287095715003460, -24.33927499327853639, 9.819080762295815390 ) ) ;
#74726=EDGE_CURVE ( 'NONE', #49130, #59761, #50916, .T. ) ;
#74727=CARTESIAN_POINT ( 'NONE',  ( 15.52975653788041122, 12.98207780544785628, 11.49999999999998934 ) ) ;
#74728=CARTESIAN_POINT ( 'NONE',  ( -69.00130780607547365, -25.29264792232144643, 5.753730642603843926 ) ) ;
#74729=CARTESIAN_POINT ( 'NONE',  ( -129.6228709571499280, -23.94994826722565406, -0.6494450866342679207 ) ) ;
#74730=EDGE_CURVE ( 'NONE', #733, #49698, #53439, .T. ) ;
#74734=CARTESIAN_POINT ( 'NONE',  ( -79.00053288248066963, -25.30543024437582034, 5.507749646993243431 ) ) ;
#74737=CARTESIAN_POINT ( 'NONE',  ( -16.72505113720834657, 11.10480813184383742, -1.500000000000002220 ) ) ;
#74738=B_SPLINE_CURVE_WITH_KNOTS ( 'NONE', 3,
 ( #85356, #98584, #37199, #14341 ),
 .UNSPECIFIED., .F., .F.,
 ( 4, 4 ),
 ( 0.7192904550652682305, 0.7202912021060337011 ),
 .UNSPECIFIED. ) ;
#74740=CARTESIAN_POINT ( 'NONE',  ( -18.19455084753484542, -10.52586660885228298, 11.49999999999999645 ) ) ;
#74742=CARTESIAN_POINT ( 'NONE',  ( -70.50643210755447399, -24.15602025860895807, 10.28564288303535967 ) ) ;
#74743=CARTESIAN_POINT ( 'NONE',  ( -17.89045161427552699, -12.92718102017995641, 11.49999999999998934 ) ) ;
#74744=EDGE_CURVE ( 'NONE', #100315, #87641, #96925, .T. ) ;
#74745=CARTESIAN_POINT ( 'NONE',  ( -39.44687923781921057, -25.31589135549187120, 4.188173601291640402 ) ) ;
#74746=B_SPLINE_CURVE_WITH_KNOTS ( 'NONE', 3,
 ( #65668, #78844, #57547, #86969 ),
 .UNSPECIFIED., .F., .F.,
 ( 4, 4 ),
 ( 0.000000000000000000, 0.0001007156686975780100 ),
 .UNSPECIFIED. ) ;
#74747=CARTESIAN_POINT ( 'NONE',  ( -47.62287095715004881, -24.50216790748205398, 0.6166512839542470648 ) ) ;
#74751=CARTESIAN_POINT ( 'NONE',  ( -31.58039431984602885, -24.51314013834316086, 0.6176544820404139546 ) ) ;
#74752=ORIENTED_EDGE ( 'NONE', *, *, #94246, .F. ) ;
#74753=ORIENTED_EDGE ( 'NONE', *, *, #11760, .T. ) ;
#74754=CARTESIAN_POINT ( 'NONE',  ( -83.62287095715007013, -24.65952944569304606, 1.056160979905700792 ) ) ;
#74756=CARTESIAN_POINT ( 'NONE',  ( -76.55011161496653926, -24.15543982623907482, -0.2315651400026599582 ) ) ;
#74758=CARTESIAN_POINT ( 'NONE',  ( -6.092534927433182368, -19.63929903328317295, -1.500000000000002220 ) ) ;
#74759=CARTESIAN_POINT ( 'NONE',  ( 16.61460563260716583, 13.71664681387569118, 11.49999999999999645 ) ) ;
#74760=ORIENTED_EDGE ( 'NONE', *, *, #90211, .T. ) ;
#74761=CARTESIAN_POINT ( 'NONE',  ( -91.62578869787175506, -24.51314013834316086, 0.6176544820404156200 ) ) ;
#74762=FACE_OUTER_BOUND ( 'NONE', #66937, .T. ) ;
#74763=CARTESIAN_POINT ( 'NONE',  ( 20.54922051473491607, -8.805037660420627077, 11.49999999999998934 ) ) ;
#74766=ORIENTED_EDGE ( 'NONE', *, *, #77612, .F. ) ;
#74767=CARTESIAN_POINT ( 'NONE',  ( -40.49165087243459737, -29.50249503729891742, 5.543933732384023649 ) ) ;
#74769=CARTESIAN_POINT ( 'NONE',  ( -17.14161228048114438, 11.91956482804130601, -1.500000000000002220 ) ) ;
#74770=ORIENTED_EDGE ( 'NONE', *, *, #170, .F. ) ;
#74771=CARTESIAN_POINT ( 'NONE',  ( -39.57784196604458771, -25.15646891919385908, 3.099756419313730138 ) ) ;
#74773=ORIENTED_EDGE ( 'NONE', *, *, #5704, .F. ) ;
#74775=CARTESIAN_POINT ( 'NONE',  ( -100.6235771386987778, -25.00182538069146787, 7.747789668545043362 ) ) ;
#74776=CARTESIAN_POINT ( 'NONE',  ( -8.144517828999388698, 19.50133175306300970, -1.500000000000002220 ) ) ;
#74778=CARTESIAN_POINT ( 'NONE',  ( -117.5877662462894904, -24.65952944569305316, 1.056160979905706343 ) ) ;
#74779=CARTESIAN_POINT ( 'NONE',  ( -71.52287095715007581, -29.50247984919015209, -1.443849546365055359 ) ) ;
#74780=CARTESIAN_POINT ( 'NONE',  ( -121.6228709571500417, -23.48783264082478794, -1.443836473390058384 ) ) ;
#74781=CARTESIAN_POINT ( 'NONE',  ( -76.50052754764180918, -24.51419770103157347, 9.386484678747176957 ) ) ;
#74782=CARTESIAN_POINT ( 'NONE',  ( -49.17699911376700328, -25.22559820935306618, 3.608295678972204268 ) ) ;
#74783=CARTESIAN_POINT ( 'NONE',  ( -19.76859095128058996, -9.124614402804876789, -1.500000000000002220 ) ) ;
#74784=CARTESIAN_POINT ( 'NONE',  ( -81.14265914342044539, -25.24759757244822467, 6.882252479551046243 ) ) ;
#74785=CARTESIAN_POINT ( 'NONE',  ( -22.12323335113916301, -3.008119206214963981, 11.49999999999999645 ) ) ;
#74787=LINE ( 'NONE', #13885, #61592 ) ;
#74788=CARTESIAN_POINT ( 'NONE',  ( -92.52287095715006160, -23.47596703998600631, 11.44779298504228393 ) ) ;
#74791=VERTEX_POINT ( 'NONE', #40660 ) ;
#74794=ORIENTED_EDGE ( 'NONE', *, *, #85854, .F. ) ;
#74797=CARTESIAN_POINT ( 'NONE',  ( -114.6228709571500559, -24.66019654487199730, 8.947790411086122830 ) ) ;
#74798=CARTESIAN_POINT ( 'NONE',  ( -78.94303308397306296, -25.03137954913951901, 5.977537200458097999 ) ) ;
#74799=CARTESIAN_POINT ( 'NONE',  ( -68.52287095715006160, -29.50250243563736774, 8.947779886222143375 ) ) ;
#74800=B_SPLINE_CURVE_WITH_KNOTS ( 'NONE', 3,
 ( #48932, #80372, #71767, #34701, #64678, #42333 ),
 .UNSPECIFIED., .F., .F.,
 ( 4, 2, 4 ),
 ( 0.000000000000000000, 0.001380901958385387677, 0.002761803916770775354 ),
 .UNSPECIFIED. ) ;
#74801=DIRECTION ( 'NONE',  ( 0.000000000000000000, -2.173523156925980399E-06, 0.9999999999976378895 ) ) ;
#74803=CARTESIAN_POINT ( 'NONE',  ( -38.52287095715009002, -23.94994826722564696, -0.6494450866342726947 ) ) ;
#74804=ORIENTED_EDGE ( 'NONE', *, *, #79972, .F. ) ;
#74805=CARTESIAN_POINT ( 'NONE',  ( 19.37663158793545293, -0.8356294931911363300, 11.49999999999999645 ) ) ;
#74806=CARTESIAN_POINT ( 'NONE',  ( -115.5228709571500190, -24.52323809116983355, 9.355190652339423707 ) ) ;
#74813=B_SPLINE_CURVE_WITH_KNOTS ( 'NONE', 3,
 ( #73239, #19437, #42310, #48404, #64653, #94561 ),
 .UNSPECIFIED., .F., .F.,
 ( 4, 2, 4 ),
 ( 0.000000000000000000, 0.001380764517854763014, 0.002761529035709526028 ),
 .UNSPECIFIED. ) ;
#74815=CARTESIAN_POINT ( 'NONE',  ( 19.11985901488480621, -4.296470200863222288, -1.500000000000002220 ) ) ;
#74816=CARTESIAN_POINT ( 'NONE',  ( -37.62287095715005592, -24.64898659630367206, 1.056161002820819261 ) ) ;
#74819=CARTESIAN_POINT ( 'NONE',  ( -14.38888013576714719, -16.06800976983558726, -1.500000000000002220 ) ) ;
#74821=CARTESIAN_POINT ( 'NONE',  ( -70.32380231474228083, -25.12219144746705268, 7.101635560771297762 ) ) ;
#74822=CARTESIAN_POINT ( 'NONE',  ( -44.62287095715004881, -29.50248528299804818, 1.056150453629031594 ) ) ;
#74824=CARTESIAN_POINT ( 'NONE',  ( -11.38079350637645959, -19.95400817559217899, -1.500000000000002220 ) ) ;
#74829=CARTESIAN_POINT ( 'NONE',  ( -19.56588111578679090, -4.897929960003377658, 11.49999999999999645 ) ) ;
#74830=CARTESIAN_POINT ( 'NONE',  ( -70.92287095715006728, -23.47593901973090169, -1.443836447538997536 ) ) ;
#74831=CARTESIAN_POINT ( 'NONE',  ( -91.52287095715010423, -24.34917612406837861, 0.1852690917426554895 ) ) ;
#74832=DIRECTION ( 'NONE',  ( 1.000000000000000000, 3.773278334444167608E-23, 8.201307833595939069E-29 ) ) ;
#74834=CARTESIAN_POINT ( 'NONE',  ( -31.23108706089061570, -23.47596703998600276, 11.44779298504227683 ) ) ;
#74835=CARTESIAN_POINT ( 'NONE',  ( 1.822157996128044299, -19.77364354024053839, 11.49999999999998934 ) ) ;
#74837=CARTESIAN_POINT ( 'NONE',  ( -19.57314199983870751, -2.777824058246878280, -1.500000000000002220 ) ) ;
#74838=CARTESIAN_POINT ( 'NONE',  ( -126.5549963774327580, -24.51419770103158058, 9.386484678747164523 ) ) ;
#74839=DIRECTION ( 'NONE',  ( -3.773278334453080206E-23, 0.9999999999976377785, 2.173523156925979975E-06 ) ) ;
#74841=CARTESIAN_POINT ( 'NONE',  ( 3.345817365282868217, 20.41450801592841557, 11.49999999999999645 ) ) ;
#74842=CARTESIAN_POINT ( 'NONE',  ( -99.62287095715005592, -29.50250786944525672, 11.44777988621623166 ) ) ;
#74843=CARTESIAN_POINT ( 'NONE',  ( -111.3776484685884327, -29.50249240399202222, 4.332395270848422797 ) ) ;
#74844=CARTESIAN_POINT ( 'NONE',  ( -75.52287095715006160, -25.00158670708909625, 2.256160236439166411 ) ) ;
#74845=CARTESIAN_POINT ( 'NONE',  ( 8.023449251107201974, -21.19570997880782670, 11.49999999999999645 ) ) ;
#74846=ORIENTED_EDGE ( 'NONE', *, *, #5396, .F. ) ;
#74847=B_SPLINE_SURFACE_WITH_KNOTS ( 'NONE', 3, 3, ( 
 ( #53695, #36954, #91237, #54198 ),
 ( #8001, #7500, #92233, #98843 ),
 ( #91732, #68903, #38949, #53193 ),
 ( #38452, #14609, #76497, #7004 ),
 ( #37951, #30335, #67922, #22706 ),
 ( #69904, #84623, #69407, #30840 ),
 ( #59811, #61806, #15608, #92726 ),
 ( #85122, #46573, #389, #83116 ),
 ( #21218, #13606, #24226, #41462 ),
 ( #85625, #40464, #9002, #18120 ) ),
 .UNSPECIFIED., .F., .F., .F.,
 ( 4, 3, 3, 4 ),
 ( 4, 4 ),
 ( 0.0004766839783816472268, 0.1491231665100170578, 0.2234464077758347711, 0.2977696490416524844 ),
 ( 0.5995664120385277851, 0.6009364153319428636 ),
 .UNSPECIFIED. ) ;
#74850=ADVANCED_FACE ( 'NONE', ( #96938 ), #89822, .F. ) ;
#74853=ORIENTED_EDGE ( 'NONE', *, *, #88458, .F. ) ;
#74854=EDGE_LOOP ( 'NONE', ( #66568, #5720, #26432, #92372 ) ) ;
#74855=CARTESIAN_POINT ( 'NONE',  ( -99.96719126485838558, -25.13541771911171807, 7.029542260679920496 ) ) ;
#74856=CARTESIAN_POINT ( 'NONE',  ( 22.85402955525884394, -0.1436109537974766814, -1.500000000000002220 ) ) ;
#74857=CARTESIAN_POINT ( 'NONE',  ( -29.58660889787569914, -24.27033885141579006, 0.1864212292069159782 ) ) ;
#74858=CARTESIAN_POINT ( 'NONE',  ( -5.754811884962036217, -20.78327508566754389, -1.500000000000002220 ) ) ;
#74859=DIRECTION ( 'NONE',  ( 1.000000000000000000, 3.773278334444166432E-23, 8.201307841325785021E-29 ) ) ;
#74860=CARTESIAN_POINT ( 'NONE',  ( -32.58953762381672448, -23.48783264082477729, -1.443836473390074371 ) ) ;
#74862=CARTESIAN_POINT ( 'NONE',  ( -3.649967738973055376, -22.27025559232234642, 11.49999999999999645 ) ) ;
#74864=CARTESIAN_POINT ( 'NONE',  ( -88.62287095715004170, -29.50250243563736774, 8.947779886222139822 ) ) ;
#74865=AXIS2_PLACEMENT_3D ( 'NONE', #84318, #43778, #36162 ) ;
#74866=CARTESIAN_POINT ( 'NONE',  ( -10.95654650054425794, 19.06054500580150446, 11.49999999999998934 ) ) ;
#74867=EDGE_CURVE ( 'NONE', #26640, #37802, #4919, .T. ) ;
#74868=CARTESIAN_POINT ( 'NONE',  ( -64.52287095715009002, -23.94994826722565406, -0.6494450866342742490 ) ) ;
#74869=FACE_OUTER_BOUND ( 'NONE', #84695, .T. ) ;
#74872=CARTESIAN_POINT ( 'NONE',  ( -90.63292611122409426, -24.40133493613050675, 9.663955038902805939 ) ) ;
#74874=CARTESIAN_POINT ( 'NONE',  ( -29.52287095715007581, -24.42901175215209619, 0.6166258780728530731 ) ) ;
#74877=CARTESIAN_POINT ( 'NONE',  ( -111.5228709571500616, -23.47596703998600631, 11.44779298504228038 ) ) ;
#74879=CARTESIAN_POINT ( 'NONE',  ( -36.60105005485234386, -23.96119346886880663, -0.6495511937832127991 ) ) ;
#74881=CARTESIAN_POINT ( 'NONE',  ( -19.81292649638395531, 4.959676026661640869, -1.500000000000002220 ) ) ;
#74882=VERTEX_POINT ( 'NONE', #36033 ) ;
#74884=CARTESIAN_POINT ( 'NONE',  ( -92.52287095715009002, -24.66019654487200086, 8.947790411086115725 ) ) ;
#74886=CARTESIAN_POINT ( 'NONE',  ( -105.5960322518042176, -23.85016227208580730, -0.8807180028928328630 ) ) ;
#74887=CARTESIAN_POINT ( 'NONE',  ( -81.42380231474228935, -25.31401921878147832, 5.197788989978542773 ) ) ;
#74888=ORIENTED_EDGE ( 'NONE', *, *, #13121, .T. ) ;
#74889=B_SPLINE_CURVE_WITH_KNOTS ( 'NONE', 3,
 ( #55905, #87843, #74115, #66532 ),
 .UNSPECIFIED., .F., .F.,
 ( 4, 4 ),
 ( 0.000000000000000000, 0.0001000000000000028644 ),
 .UNSPECIFIED. ) ;
#74891=CARTESIAN_POINT ( 'NONE',  ( -94.55620429048340725, -23.47593901973091235, -1.443836447539002865 ) ) ;
#74893=CARTESIAN_POINT ( 'NONE',  ( 19.40640353424967302, -7.489167304209242815, -1.500000000000002220 ) ) ;
#74896=ORIENTED_EDGE ( 'NONE', *, *, #61948, .F. ) ;
#74897=CARTESIAN_POINT ( 'NONE',  ( -68.52287095715004739, -24.50321055353805733, 9.387540953477525818 ) ) ;
#74899=EDGE_LOOP ( 'NONE', ( #94847, #45922, #46332, #52295 ) ) ;
#74902=CARTESIAN_POINT ( 'NONE',  ( -116.4728709570019873, -25.30556170156494744, 4.804051544042277300 ) ) ;
#74903=CARTESIAN_POINT ( 'NONE',  ( -60.52287095715006160, -23.48786465467241058, 11.44779295918254824 ) ) ;
#74904=CARTESIAN_POINT ( 'NONE',  ( -71.30457154551152144, -25.31201785239418456, 6.209207263561717483 ) ) ;
#74905=CARTESIAN_POINT ( 'NONE',  ( 20.51613352552997327, 8.347415244503286758, 11.49999999999999645 ) ) ;
#74906=EDGE_LOOP ( 'NONE', ( #31185, #99457, #37100, #64197 ) ) ;
#74907=CARTESIAN_POINT ( 'NONE',  ( -88.88918693012689687, -25.26877915520014639, 5.947789088310639904 ) ) ;
#74908=CARTESIAN_POINT ( 'NONE',  ( 22.24477432615492134, 4.004077059304647968, -1.500000000000002220 ) ) ;
#74909=CARTESIAN_POINT ( 'NONE',  ( -115.5889401794561024, -24.63419186844613051, 9.035850630976923981 ) ) ;
#74911=EDGE_CURVE ( 'NONE', #25435, #84515, #83614, .T. ) ;
#74914=EDGE_CURVE ( 'NONE', #44615, #30450, #4096, .T. ) ;
#74916=CARTESIAN_POINT ( 'NONE',  ( -78.62287095715005592, -24.64965695001468404, 8.947790433994182280 ) ) ;
#74917=VERTEX_POINT ( 'NONE', #67494 ) ;
#74919=CARTESIAN_POINT ( 'NONE',  ( 2.321567282091853812, -22.14299765706108403, -1.500000000000002220 ) ) ;
#74921=ORIENTED_EDGE ( 'NONE', *, *, #95204, .F. ) ;
#74923=CARTESIAN_POINT ( 'NONE',  ( -81.32299058106391954, -25.08345032616901094, 7.319022766874549113 ) ) ;
#74924=CARTESIAN_POINT ( 'NONE',  ( -25.63723411449804246, -24.85022734580098458, 3.654579668448656005 ) ) ;
#74925=CARTESIAN_POINT ( 'NONE',  ( -103.5228709571500758, -23.72773821059536203, 11.05748984161097326 ) ) ;
#74927=CARTESIAN_POINT ( 'NONE',  ( -1.849579639615634097, -19.42000222497389927, -1.500000000000002220 ) ) ;
#74929=CARTESIAN_POINT ( 'NONE',  ( -11.48222599368078889, -18.13851731312990267, -1.500000000000002220 ) ) ;
#74932=CARTESIAN_POINT ( 'NONE',  ( -65.52287095715006160, -25.00182538069144655, 7.747789668545101982 ) ) ;
#74933=CARTESIAN_POINT ( 'NONE',  ( 22.80427751693360960, 0.003464389817739472934, -1.500000000000002220 ) ) ;
#74934=ADVANCED_FACE ( 'NONE', ( #12689 ), #66518, .F. ) ;
#74938=CARTESIAN_POINT ( 'NONE',  ( -125.5228709571500616, -23.48783264083375144, -1.443836473376139740 ) ) ;
#74939=CARTESIAN_POINT ( 'NONE',  ( -19.26508835251014773, 5.270845654819066084, 11.49999999999999645 ) ) ;
#74940=CARTESIAN_POINT ( 'NONE',  ( -50.52287095715007581, -24.15431212366388891, -0.2830839119429292561 ) ) ;
#74941=CARTESIAN_POINT ( 'NONE',  ( -74.62362437411805161, -24.66019654487199730, 8.947790411086108620 ) ) ;
#74942=CARTESIAN_POINT ( 'NONE',  ( -108.6228709571500559, -23.47593901973091235, -1.443836447538999312 ) ) ;
#74944=CARTESIAN_POINT ( 'NONE',  ( -69.62287095715005592, -29.50250243563736774, 8.947779886222143375 ) ) ;
#74945=CARTESIAN_POINT ( 'NONE',  ( -92.62287095715005592, -24.65952944569304606, 1.056160979905700348 ) ) ;
#74946=CARTESIAN_POINT ( 'NONE',  ( -17.03913561245058261, -13.47071831616118942, 11.49999999999998934 ) ) ;
#74948=CARTESIAN_POINT ( 'NONE',  ( -37.55620429048340014, -23.47593901973091235, -1.443836447539011525 ) ) ;
#74949=CARTESIAN_POINT ( 'NONE',  ( 19.50827032651345405, -1.201405007418623994, -1.500000000000002220 ) ) ;
#74950=EDGE_CURVE ( 'NONE', #55465, #39871, #44649, .T. ) ;
#74953=ORIENTED_EDGE ( 'NONE', *, *, #96604, .T. ) ;
#74955=EDGE_CURVE ( 'NONE', #19969, #3731, #47321, .T. ) ;
#74957=CARTESIAN_POINT ( 'NONE',  ( -108.8968792378191921, -25.14264220134206695, 6.986250900936221697 ) ) ;
#74958=CARTESIAN_POINT ( 'NONE',  ( -40.62287095715005592, -23.47593901973091235, -1.443836447539011525 ) ) ;
#74959=CARTESIAN_POINT ( 'NONE',  ( -20.49763986188970932, -1.003951800832726615, 11.49999999999999645 ) ) ;
#74960=CARTESIAN_POINT ( 'NONE',  ( -47.52287095715006160, -23.48786465467240347, 11.44779295918255002 ) ) ;
#74961=CARTESIAN_POINT ( 'NONE',  ( -42.62287095715004881, -24.66019654487199020, 8.947790411086135265 ) ) ;
#74962=AXIS2_PLACEMENT_3D ( 'NONE', #31920, #61877, #1978 ) ;
#74964=CARTESIAN_POINT ( 'NONE',  ( -62.52287095715009002, -23.72773821059535848, 11.05748984161097503 ) ) ;
#74968=ADVANCED_FACE ( 'NONE', ( #74106 ), #22781, .F. ) ;
#74969=CARTESIAN_POINT ( 'NONE',  ( -61.62287095715002749, -23.94994826722515668, -0.6494450866351731966 ) ) ;
#74970=EDGE_LOOP ( 'NONE', ( #12002, #24372, #23167, #29846 ) ) ;
#74972=CARTESIAN_POINT ( 'NONE',  ( 20.35648204094723468, -10.72454223111430593, 11.49999999999999645 ) ) ;
#74973=CARTESIAN_POINT ( 'NONE',  ( -4.239441843796335263, -22.36999388947090139, -1.500000000000002220 ) ) ;
#74978=CARTESIAN_POINT ( 'NONE',  ( -40.52287095715006870, -23.48786465467241058, 11.44779295918255180 ) ) ;
#74979=CARTESIAN_POINT ( 'NONE',  ( -99.19454649804008284, -25.30157761398589500, 5.270710036488496009 ) ) ;
#74980=CARTESIAN_POINT ( 'NONE',  ( 15.10893391618534665, -15.86458014800626692, -1.500000000000002220 ) ) ;
#74981=ADVANCED_FACE ( 'NONE', ( #76575 ), #99903, .T. ) ;
#74984=CARTESIAN_POINT ( 'NONE',  ( -34.58953762381673158, -24.66019654487199375, 8.947790411086135265 ) ) ;
#74985=EDGE_CURVE ( 'NONE', #53498, #21106, #463, .T. ) ;
#74988=LINE ( 'NONE', #97831, #84170 ) ;
#74990=CARTESIAN_POINT ( 'NONE',  ( 1.945971545120378288, -20.36639758168144709, -1.500000000000002220 ) ) ;
#74992=ORIENTED_EDGE ( 'NONE', *, *, #33291, .T. ) ;
#74994=VERTEX_POINT ( 'NONE', #14685 ) ;
#74995=CARTESIAN_POINT ( 'NONE',  ( 11.60186680256600233, 19.91347440808847935, 11.49999999999998934 ) ) ;
#74996=CARTESIAN_POINT ( 'NONE',  ( -61.61074830552635717, -23.48783264082476663, -1.443836473390096575 ) ) ;
#74997=EDGE_CURVE ( 'NONE', #17101, #14971, #85199, .T. ) ;
#74998=CARTESIAN_POINT ( 'NONE',  ( -14.42758394406654610, -14.16023863206117994, -1.500000000000002220 ) ) ;
#74999=VECTOR ( 'NONE', #34611, 1000.000000000000114 ) ;
#75000=ORIENTED_EDGE ( 'NONE', *, *, #58385, .F. ) ;
#75004=CARTESIAN_POINT ( 'NONE',  ( -51.52287095715009002, -23.48783264082477018, -1.443836473390092578 ) ) ;
#75005=CARTESIAN_POINT ( 'NONE',  ( -99.62530823664367574, -24.51419770103158413, 9.386484678747175181 ) ) ;
#75006=CARTESIAN_POINT ( 'NONE',  ( -20.52298544035203776, 6.160189734329080125, 11.49999999999999645 ) ) ;
#75010=EDGE_LOOP ( 'NONE', ( #64747, #62692, #43248, #79270 ) ) ;
#75011=CARTESIAN_POINT ( 'NONE',  ( -0.2510023010970363067, -20.70922355669356563, -1.500000000000002220 ) ) ;
#75012=EDGE_LOOP ( 'NONE', ( #86507, #10489, #15378, #25355 ) ) ;
#75014=VERTEX_POINT ( 'NONE', #62894 ) ;
#75017=CARTESIAN_POINT ( 'NONE',  ( 20.71091302404612833, 3.140364381853995912, -1.500000000000002220 ) ) ;
#75018=CARTESIAN_POINT ( 'NONE',  ( 21.77894307773758698, -2.757304969434911879, 11.49999999999999645 ) ) ;
#75019=CARTESIAN_POINT ( 'NONE',  ( -91.55620429048339304, -24.65952944569304606, 1.056160979905700792 ) ) ;
#75020=CARTESIAN_POINT ( 'NONE',  ( -3.310667818835141940, 22.29536907041311977, -1.500000000000002220 ) ) ;
#75021=CARTESIAN_POINT ( 'NONE',  ( -19.40599490818632233, 7.965113791304038848, 11.49999999999998934 ) ) ;
#75023=CARTESIAN_POINT ( 'NONE',  ( -119.5902191003218036, -24.15620529776629510, 10.23563542870659582 ) ) ;
#75026=ADVANCED_FACE ( 'NONE', ( #7080 ), #23184, .T. ) ;
#75030=ORIENTED_EDGE ( 'NONE', *, *, #29467, .F. ) ;
#75031=CARTESIAN_POINT ( 'NONE',  ( -66.60922468828853482, -23.48783264082476308, -1.443836473390097463 ) ) ;
#75032=CARTESIAN_POINT ( 'NONE',  ( 3.930203739357332360, 21.12693704021120666, -1.500000000000002220 ) ) ;
#75035=B_SPLINE_CURVE_WITH_KNOTS ( 'NONE', 3,
 ( #23785, #956, #31908, #77061 ),
 .UNSPECIFIED., .F., .F.,
 ( 4, 4 ),
 ( 0.8493875703647875142, 0.8503883174055528738 ),
 .UNSPECIFIED. ) ;
#75036=CARTESIAN_POINT ( 'NONE',  ( -91.52287095715010423, -24.66019654487199730, 8.947790411086115725 ) ) ;
#75037=ORIENTED_EDGE ( 'NONE', *, *, #71872, .T. ) ;
#75038=CARTESIAN_POINT ( 'NONE',  ( 16.98782256641479904, -12.52229676876588371, 11.49999999999998934 ) ) ;
#75040=CARTESIAN_POINT ( 'NONE',  ( -64.58350591778255989, -24.51314013834315730, 0.6176544820404094027 ) ) ;
#75044=CARTESIAN_POINT ( 'NONE',  ( 7.254013858510784729, 20.86747967231135803, -1.500000000000002220 ) ) ;
#75047=CARTESIAN_POINT ( 'NONE',  ( -51.93075163254042792, -25.24860253703637269, 6.142475047348883166 ) ) ;
#75049=CARTESIAN_POINT ( 'NONE',  ( -43.62287095715007723, -24.34917612406837861, 0.1852690917426608463 ) ) ;
#75051=CARTESIAN_POINT ( 'NONE',  ( -1.307668758097810358, 19.38731951181482671, 11.49999999999998934 ) ) ;
#75052=CARTESIAN_POINT ( 'NONE',  ( 18.88549913130557556, 9.949676122998861061, -1.500000000000002220 ) ) ;
#75053=CARTESIAN_POINT ( 'NONE',  ( -80.64675904551151575, -29.50249039766296022, 3.409318347773680369 ) ) ;
#75054=LINE ( 'NONE', #42645, #75419 ) ;
#75055=CARTESIAN_POINT ( 'NONE',  ( -64.52209052475978979, -23.48786465467241058, 11.44779295918254824 ) ) ;
#75056=CARTESIAN_POINT ( 'NONE',  ( -129.5228709571500758, -29.50250243563736774, 8.947779886222132717 ) ) ;
#75057=CARTESIAN_POINT ( 'NONE',  ( 14.74224262856723833, 17.19160420931263999, -1.500000000000002220 ) ) ;
#75059=B_SPLINE_SURFACE_WITH_KNOTS ( 'NONE', 3, 3, ( 
 ( #9723, #53901, #71126, #46279 ),
 ( #1112, #93949, #32053, #77207 ),
 ( #71629, #48292, #24436, #7712 ),
 ( #79222, #85330, #84835, #78704 ),
 ( #40175, #23417, #46783, #62514 ),
 ( #63025, #9210, #32554, #63527 ),
 ( #15316, #38660, #69626, #62011 ) ),
 .UNSPECIFIED., .F., .F., .F.,
 ( 4, 3, 4 ),
 ( 4, 4 ),
 ( 0.0004766839783817475697, 0.1029713700210893867, 0.2054660560637970312 ),
 ( 0.4696134588889684935, 0.4708428622320510182 ),
 .UNSPECIFIED. ) ;
#75061=CARTESIAN_POINT ( 'NONE',  ( -110.2228709571500787, -23.47593901973090169, -1.443836447538996648 ) ) ;
#75062=LINE ( 'NONE', #34528, #76755 ) ;
#75063=CARTESIAN_POINT ( 'NONE',  ( -19.53060160647804722, 3.385818350044136338, 11.49999999999999645 ) ) ;
#75064=CARTESIAN_POINT ( 'NONE',  ( -50.52287095715006160, -25.00158670708909270, 2.256160236439166411 ) ) ;
#75065=DIRECTION ( 'NONE',  ( -3.773278334453079030E-23, 0.9999999999976377785, 2.173523156925979128E-06 ) ) ;
#75066=VERTEX_POINT ( 'NONE', #10082 ) ;
#75068=CARTESIAN_POINT ( 'NONE',  ( -28.54389657640137656, -25.26026329057766517, 1.825711730509220976 ) ) ;
#75071=EDGE_CURVE ( 'NONE', #68524, #83417, #34423, .T. ) ;
#75072=CARTESIAN_POINT ( 'NONE',  ( 19.98343133220876666, -8.209121646405339590, 11.49999999999998934 ) ) ;
#75073=ADVANCED_FACE ( 'NONE', ( #86207 ), #25300, .F. ) ;
#75074=CARTESIAN_POINT ( 'NONE',  ( -99.62287095715005592, -23.96127896941631619, -0.6493128931037778218 ) ) ;
#75075=CARTESIAN_POINT ( 'NONE',  ( -101.6228709571500559, -23.48786465467242479, 11.44779295918254114 ) ) ;
#75076=EDGE_CURVE ( 'NONE', #93093, #13115, #21954, .T. ) ;
#75078=LINE ( 'NONE', #98411, #18267 ) ;
#75079=CARTESIAN_POINT ( 'NONE',  ( -19.37706247964952411, -4.161318200553020041, -1.500000000000002220 ) ) ;
#75080=B_SPLINE_CURVE_WITH_KNOTS ( 'NONE', 3,
 ( #20383, #82297, #14266, #27525, #74680, #21377, #45242, #37618 ),
 .UNSPECIFIED., .F., .F.,
 ( 4, 2, 2, 4 ),
 ( -0.001224554619866346930, -0.0002241820295893657503, 0.0007761905606876154298, 0.002776935741241573670 ),
 .UNSPECIFIED. ) ;
#75081=ORIENTED_EDGE ( 'NONE', *, *, #99278, .F. ) ;
#75082=VECTOR ( 'NONE', #23669, 1000.000000000000114 ) ;
#75083=EDGE_CURVE ( 'NONE', #29468, #66746, #57043, .T. ) ;
#75084=CARTESIAN_POINT ( 'NONE',  ( -11.07518157712430096, -17.02944518001645946, 11.49999999999999645 ) ) ;
#75086=B_SPLINE_CURVE_WITH_KNOTS ( 'NONE', 3,
 ( #89432, #20395, #59482, #98521 ),
 .UNSPECIFIED., .F., .F.,
 ( 4, 4 ),
 ( 0.09882728979063827579, 0.09982803683140384354 ),
 .UNSPECIFIED. ) ;
#75087=PLANE ( 'NONE',  #68432 ) ;
#75088=ORIENTED_EDGE ( 'NONE', *, *, #52482, .F. ) ;
#75089=CARTESIAN_POINT ( 'NONE',  ( -107.5228709571500758, -23.48786465467241769, 11.44779295918253936 ) ) ;
#75093=CARTESIAN_POINT ( 'NONE',  ( -51.48668340319347436, -25.21911759177204715, 6.451348099842415529 ) ) ;
#75094=CARTESIAN_POINT ( 'NONE',  ( 2.879247915899910470, -19.84986158617241614, -1.500000000000002220 ) ) ;
#75095=EDGE_CURVE ( 'NONE', #25724, #28213, #66763, .T. ) ;
#75100=EDGE_CURVE ( 'NONE', #24828, #2526, #9582, .T. ) ;
#75101=CARTESIAN_POINT ( 'NONE',  ( -0.9063223138645676302, -22.79912562917415997, 11.49999999999999645 ) ) ;
#75109=CARTESIAN_POINT ( 'NONE',  ( -9.774569144048079750, -20.17623354167628946, 11.49999999999999645 ) ) ;
#75111=VERTEX_POINT ( 'NONE', #72995 ) ;
#75112=CARTESIAN_POINT ( 'NONE',  ( 6.737473828552405841, -19.20966278261563076, -1.500000000000002220 ) ) ;
#75115=CARTESIAN_POINT ( 'NONE',  ( -11.38079350637645959, -19.95400817559217899, -1.500000000000002220 ) ) ;
#75116=ADVANCED_FACE ( 'NONE', ( #57285 ), #95320, .F. ) ;
#75117=PLANE ( 'NONE',  #95470 ) ;
#75118=VERTEX_POINT ( 'NONE', #1483 ) ;
#75119=B_SPLINE_CURVE_WITH_KNOTS ( 'NONE', 3,
 ( #53658, #86087, #54652, #55661 ),
 .UNSPECIFIED., .F., .F.,
 ( 4, 4 ),
 ( 0.000000000000000000, 9.999999999998897304E-05 ),
 .UNSPECIFIED. ) ;
#75120=CARTESIAN_POINT ( 'NONE',  ( -89.55620429048337883, -23.48783264082478794, -1.443836473390065045 ) ) ;
#75121=ADVANCED_FACE ( 'NONE', ( #70992 ), #10577, .T. ) ;
#75122=CARTESIAN_POINT ( 'NONE',  ( -77.51233885098207566, -23.96169478059713498, 10.65365249895717703 ) ) ;
#75125=CARTESIAN_POINT ( 'NONE',  ( -20.86817740539179056, 4.147639786170328691, 11.49999999999999645 ) ) ;
#75126=ORIENTED_EDGE ( 'NONE', *, *, #73135, .F. ) ;
#75127=B_SPLINE_CURVE_WITH_KNOTS ( 'NONE', 3,
 ( #18802, #64016, #70592, #80712 ),
 .UNSPECIFIED., .F., .F.,
 ( 4, 4 ),
 ( 0.06976270681042859301, 1.000000000000000000 ),
 .UNSPECIFIED. ) ;
#75129=CARTESIAN_POINT ( 'NONE',  ( -10.57539506955483333, 19.50334513348995813, 11.49999999999998934 ) ) ;
#75130=CARTESIAN_POINT ( 'NONE',  ( -18.80638259998596951, 8.471300643254643603, 11.49999999999998934 ) ) ;
#75134=CARTESIAN_POINT ( 'NONE',  ( -55.52287095715006870, -23.47596703998600631, 11.44779298504228926 ) ) ;
#75135=ORIENTED_EDGE ( 'NONE', *, *, #3220, .F. ) ;
#75137=VERTEX_POINT ( 'NONE', #63902 ) ;
#75138=CARTESIAN_POINT ( 'NONE',  ( -124.4728709571500360, -25.30558663486635851, 5.000950659935021747 ) ) ;
#75139=CARTESIAN_POINT ( 'NONE',  ( -46.52287095715006870, -24.50216790748203621, 0.6166512839542526159 ) ) ;
#75141=CARTESIAN_POINT ( 'NONE',  ( 6.562613027033147084, 19.67253995144353240, -1.500000000000002220 ) ) ;
#75142=CARTESIAN_POINT ( 'NONE',  ( -21.62197530259306788, 2.132803791230205359, 11.49999999999999645 ) ) ;
#75143=VERTEX_POINT ( 'NONE', #79082 ) ;
#75145=CARTESIAN_POINT ( 'NONE',  ( -40.62552394256396582, -25.31583768111513066, 5.067902445723437843 ) ) ;
#75147=CARTESIAN_POINT ( 'NONE',  ( -115.5935074813547629, -23.85016227208580730, -0.8807180028928280890 ) ) ;
#75148=CARTESIAN_POINT ( 'NONE',  ( 9.841385673706204429, 20.17164819615926064, 11.49999999999998934 ) ) ;
#75149=CARTESIAN_POINT ( 'NONE',  ( -50.95636528269795207, -25.31296727064691510, 4.561343259994464105 ) ) ;
#75153=VECTOR ( 'NONE', #96782, 1000.000000000000114 ) ;
#75154=ORIENTED_EDGE ( 'NONE', *, *, #55981, .F. ) ;
#75156=CARTESIAN_POINT ( 'NONE',  ( -46.61533402018017114, -23.48786465467240703, 11.44779295918255180 ) ) ;
#75158=CARTESIAN_POINT ( 'NONE',  ( -9.338289970059909351, 19.12570833482435617, -1.500000000000002220 ) ) ;
#75162=CARTESIAN_POINT ( 'NONE',  ( -20.81348254183067681, -2.960215062046979373, -1.500000000000002220 ) ) ;
#75163=PLANE ( 'NONE',  #66043 ) ;
#75164=CARTESIAN_POINT ( 'NONE',  ( 9.008567143757492346, 20.83016157428379955, 11.49999999999998934 ) ) ;
#75167=CARTESIAN_POINT ( 'NONE',  ( 13.84421170697429737, -16.98027460053469895, -1.500000000000002220 ) ) ;
#75171=VERTEX_POINT ( 'NONE', #2987 ) ;
#75172=CARTESIAN_POINT ( 'NONE',  ( -84.63259752206350583, -24.15620529776628445, 10.23563542870660292 ) ) ;
#75174=CARTESIAN_POINT ( 'NONE',  ( -20.41827678953962888, -23.96516754450130549, 1.363349870542264863 ) ) ;
#75175=CARTESIAN_POINT ( 'NONE',  ( -18.72683625574626376, -10.08736549105613278, -1.500000000000002220 ) ) ;
#75176=CARTESIAN_POINT ( 'NONE',  ( -112.5175298555210190, -24.15543982623908192, -0.2315651400026420004 ) ) ;
#75177=CARTESIAN_POINT ( 'NONE',  ( -26.71643515402310953, -24.97064495862396427, 2.706679050326408653 ) ) ;
#75178=CARTESIAN_POINT ( 'NONE',  ( -85.64374433404715603, -23.85016227208579664, -0.8807180028928370819 ) ) ;
#75179=CARTESIAN_POINT ( 'NONE',  ( -33.54542880383117875, -24.15543982623906771, -0.2315651400026580431 ) ) ;
#75180=CARTESIAN_POINT ( 'NONE',  ( -39.62287095715004881, -24.51387760970725793, 9.387446482453437824 ) ) ;
#75183=CARTESIAN_POINT ( 'NONE',  ( -6.723608784814384620, 18.44229941887336821, 11.49999999999999645 ) ) ;
#75185=ADVANCED_FACE ( 'NONE', ( #88216 ), #96320, .T. ) ;
#75186=CARTESIAN_POINT ( 'NONE',  ( -90.25937923781921768, -25.26877915520014994, 5.947789088310639904 ) ) ;
#75188=EDGE_CURVE ( 'NONE', #38852, #86526, #44023, .T. ) ;
#75189=CARTESIAN_POINT ( 'NONE',  ( -68.97793375987197351, -25.27731752798380072, 5.835604325072999643 ) ) ;
#75192=CARTESIAN_POINT ( 'NONE',  ( -27.51938903004329617, -24.63785229949931121, 8.245938776320086205 ) ) ;
#75194=CARTESIAN_POINT ( 'NONE',  ( -31.62287095715005236, -24.64898659630367206, 1.056161002820817485 ) ) ;
#75195=CARTESIAN_POINT ( 'NONE',  ( -18.76583335001664565, 6.068782795689376286, -1.500000000000002220 ) ) ;
#75196=B_SPLINE_CURVE_WITH_KNOTS ( 'NONE', 3,
 ( #92399, #30504, #44747, #37122, #59472, #98510, #68082, #22872 ),
 .UNSPECIFIED., .F., .F.,
 ( 4, 2, 2, 4 ),
 ( -0.001240666984356060066, -0.0002401179793396629458, 0.0007604310256767341739, 0.002761529035709528630 ),
 .UNSPECIFIED. ) ;
#75197=ORIENTED_EDGE ( 'NONE', *, *, #54005, .T. ) ;
#75198=B_SPLINE_CURVE_WITH_KNOTS ( 'NONE', 3,
 ( #57277, #42042, #88705, #89202, #71488, #48152 ),
 .UNSPECIFIED., .F., .F.,
 ( 4, 2, 4 ),
 ( 6.391158118966175555E-06, 0.001387004593080783544, 0.002767618028042600695 ),
 .UNSPECIFIED. ) ;
#75203=ORIENTED_EDGE ( 'NONE', *, *, #78088, .T. ) ;
#75205=CARTESIAN_POINT ( 'NONE',  ( -36.62287095715005592, -23.48786465467240347, 11.44779295918255180 ) ) ;
#75206=CARTESIAN_POINT ( 'NONE',  ( -55.65727489617320600, -23.85016227208578954, -0.8807180028928371929 ) ) ;
#75209=CARTESIAN_POINT ( 'NONE',  ( -69.96836528472165639, -25.24515055822771004, 5.376154610849502191 ) ) ;
#75210=CARTESIAN_POINT ( 'NONE',  ( -85.58953762381672448, -25.00158670708909625, 2.256160236439166411 ) ) ;
#75211=CARTESIAN_POINT ( 'NONE',  ( 6.038693664686949347, 19.05185810397003721, 11.49999999999998934 ) ) ;
#75213=AXIS2_PLACEMENT_3D ( 'NONE', #73143, #51295, #97465 ) ;
#75214=CARTESIAN_POINT ( 'NONE',  ( -100.3793702452611285, -25.27532861982699330, 2.834177754712485342 ) ) ;
#75215=CARTESIAN_POINT ( 'NONE',  ( -0.1426030150137709562, -21.20389190742572083, 11.50200000000000422 ) ) ;
#75217=CARTESIAN_POINT ( 'NONE',  ( -29.52287095715005449, -24.25394151242297980, 0.1849423911881836469 ) ) ;
#75220=CARTESIAN_POINT ( 'NONE',  ( -119.5565861874301135, -23.73766607897670866, -1.055555164236450016 ) ) ;
#75221=CARTESIAN_POINT ( 'NONE',  ( -80.56574517205659447, -23.48786465467241058, 11.44779295918254824 ) ) ;
#75223=CARTESIAN_POINT ( 'NONE',  ( -107.6228709571500701, -24.66019654487199730, 8.947790411086124607 ) ) ;
#75224=CARTESIAN_POINT ( 'NONE',  ( -119.6228709571500559, -23.72747288104469732, -1.053458166803224350 ) ) ;
#75226=ORIENTED_EDGE ( 'NONE', *, *, #80705, .T. ) ;
#75227=CARTESIAN_POINT ( 'NONE',  ( -64.62287095715005592, -23.48783264082478084, -1.443836473390069042 ) ) ;
#75229=ORIENTED_EDGE ( 'NONE', *, *, #62024, .F. ) ;
#75230=CARTESIAN_POINT ( 'NONE',  ( -20.27173212042777806, -0.06527795377243154895, 11.49999999999998934 ) ) ;
#75231=B_SPLINE_CURVE_WITH_KNOTS ( 'NONE', 3,
 ( #80255, #18848, #49828, #11243 ),
 .UNSPECIFIED., .F., .F.,
 ( 4, 4 ),
 ( 0.000000000000000000, 9.999999999998897304E-05 ),
 .UNSPECIFIED. ) ;
#75233=CARTESIAN_POINT ( 'NONE',  ( -106.5228709571500332, -23.48783264082477018, -1.443836473390085695 ) ) ;
#75236=ORIENTED_EDGE ( 'NONE', *, *, #31659, .F. ) ;
#75237=DIRECTION ( 'NONE',  ( 0.000000000000000000, -0.9999999999976377785, -2.173523156925979975E-06 ) ) ;
#75238=DIRECTION ( 'NONE',  ( 0.000000000000000000, -0.9999999999976377785, -2.173523156925979975E-06 ) ) ;
#75239=CARTESIAN_POINT ( 'NONE',  ( 10.48293302797296356, 17.13603372422173976, -1.500000000000002220 ) ) ;
#75240=CARTESIAN_POINT ( 'NONE',  ( 12.56776941831905070, -16.83212535568997126, 11.49999999999999645 ) ) ;
#75243=CARTESIAN_POINT ( 'NONE',  ( -70.62988891066373753, -24.73531770709095312, 8.716586749053508498 ) ) ;
#75244=CARTESIAN_POINT ( 'NONE',  ( 7.254013858510784729, 20.86747967231135803, -1.500000000000002220 ) ) ;
#75245=EDGE_CURVE ( 'NONE', #19866, #24503, #35301, .T. ) ;
#75246=CARTESIAN_POINT ( 'NONE',  ( 17.35315496411208613, -10.91789592880838811, -1.500000000000002220 ) ) ;
#75247=CARTESIAN_POINT ( 'NONE',  ( -96.52287095715007581, -23.47593901973090524, -1.443836447538996648 ) ) ;
#75248=CARTESIAN_POINT ( 'NONE',  ( -58.62287095715004881, -29.50250243563736774, 8.947779886222145151 ) ) ;
#75251=CARTESIAN_POINT ( 'NONE',  ( -82.62287095715004170, -23.47596703998600631, 11.44779298504227860 ) ) ;
#75252=B_SPLINE_SURFACE_WITH_KNOTS ( 'NONE', 3, 3, ( 
 ( #90698, #82585, #98291, #32293 ),
 ( #46522, #844, #39903, #7951 ),
 ( #61761, #76953, #31799, #23160 ),
 ( #9456, #47029, #69358, #92680 ),
 ( #40413, #69861, #78452, #78955 ),
 ( #99777, #1358, #54152, #93183 ),
 ( #77945, #22661, #84573, #53649 ) ),
 .UNSPECIFIED., .F., .F., .F.,
 ( 4, 3, 4 ),
 ( 4, 4 ),
 ( 0.7945040050992239200, 0.8970133687736498995, 0.9995227324480758790 ),
 ( 0.3895929982246983947, 0.3907855847607153987 ),
 .UNSPECIFIED. ) ;
#75254=ORIENTED_EDGE ( 'NONE', *, *, #48399, .F. ) ;
#75257=CARTESIAN_POINT ( 'NONE',  ( -89.62287095715004170, -23.48786465467241413, 11.44779295918254114 ) ) ;
#75258=CARTESIAN_POINT ( 'NONE',  ( -76.54259362716096859, -24.51314013834316441, 0.6176544820404193947 ) ) ;
#75259=CARTESIAN_POINT ( 'NONE',  ( -20.17529555308526668, -4.016306826964139098, -1.500000000000002220 ) ) ;
#75260=CARTESIAN_POINT ( 'NONE',  ( -21.50746323947805649, 1.722430922125298247, 11.49999999999999645 ) ) ;
#75263=DIRECTION ( 'NONE',  ( -1.000000000000000000, -3.773278334444167608E-23, -8.201307833595939069E-29 ) ) ;
#75264=CARTESIAN_POINT ( 'NONE',  ( 8.681249458320607459, -20.60847208623538762, -1.500000000000002220 ) ) ;
#75265=CARTESIAN_POINT ( 'NONE',  ( -79.53472330195882023, -25.12205703624572095, 6.603901019741583056 ) ) ;
#75268=CARTESIAN_POINT ( 'NONE',  ( -105.6228709571500417, -24.99156045073393173, 7.747789690856161648 ) ) ;
#75269=CARTESIAN_POINT ( 'NONE',  ( -49.56034792530066824, -23.73791477778911840, 11.05961554403170943 ) ) ;
#75270=CARTESIAN_POINT ( 'NONE',  ( -20.64841573231975147, 3.066018724555340746, -1.500000000000002220 ) ) ;
#75271=ORIENTED_EDGE ( 'NONE', *, *, #71038, .T. ) ;
#75272=VECTOR ( 'NONE', #93945, 1000.000000000000114 ) ;
#75273=CARTESIAN_POINT ( 'NONE',  ( -67.63120879115606954, -24.35071581493543746, 9.817618358456023486 ) ) ;
#75274=ORIENTED_EDGE ( 'NONE', *, *, #69941, .F. ) ;
#75277=CARTESIAN_POINT ( 'NONE',  ( 20.99878002148846790, -2.064974809011826729, -1.500000000000002220 ) ) ;
#75280=CARTESIAN_POINT ( 'NONE',  ( -48.87844976791110696, -25.26434452170244072, 6.005111483681883300 ) ) ;
#75281=CARTESIAN_POINT ( 'NONE',  ( -86.62287095715004170, -29.50250786944525672, 11.44777988621623344 ) ) ;
#75283=CARTESIAN_POINT ( 'NONE',  ( -79.39903364703884847, -25.24308088847154963, 6.330656792118257492 ) ) ;
#75284=CARTESIAN_POINT ( 'NONE',  ( -13.65724274058436194, -16.95215541261048742, -1.500000000000002220 ) ) ;
#75285=CARTESIAN_POINT ( 'NONE',  ( -71.49027787591442973, -25.24674164662046394, 5.369049284096080399 ) ) ;
#75286=CARTESIAN_POINT ( 'NONE',  ( 19.83320176327591255, -10.20924650237717835, 11.49999999999999645 ) ) ;
#75287=ORIENTED_EDGE ( 'NONE', *, *, #99360, .T. ) ;
#75288=CARTESIAN_POINT ( 'NONE',  ( -45.62287095715004881, -23.48783264082478084, -1.443836473390070374 ) ) ;
#75290=CARTESIAN_POINT ( 'NONE',  ( -36.55620429048339304, -23.48786465467240347, 11.44779295918255180 ) ) ;
#75291=ORIENTED_EDGE ( 'NONE', *, *, #983, .F. ) ;
#75292=VECTOR ( 'NONE', #18485, 1000.000000000000114 ) ;
#75294=ORIENTED_EDGE ( 'NONE', *, *, #11965, .F. ) ;
#75295=CARTESIAN_POINT ( 'NONE',  ( -28.52287095715005094, -23.31182002239687989, -1.443836447538998202 ) ) ;
#75299=CARTESIAN_POINT ( 'NONE',  ( -12.28997142660015740, 14.97987746540053422, 11.49999999999998934 ) ) ;
#75300=CARTESIAN_POINT ( 'NONE',  ( -31.52287095715006160, -23.73934037231756022, 11.05740245334329686 ) ) ;
#75301=ORIENTED_EDGE ( 'NONE', *, *, #46228, .F. ) ;
#75303=CARTESIAN_POINT ( 'NONE',  ( 4.312616920666290987, -18.91975033782923887, 11.49999999999999645 ) ) ;
#75304=CARTESIAN_POINT ( 'NONE',  ( -129.6228709571500417, -29.50247984919015209, -1.443849546365044922 ) ) ;
#75305=ORIENTED_EDGE ( 'NONE', *, *, #60336, .T. ) ;
#75307=EDGE_CURVE ( 'NONE', #85611, #7766, #96815, .T. ) ;
#75309=DIRECTION ( 'NONE',  ( -0.7297249646783463550, 1.486126453139760626E-06, -0.6837407958597889746 ) ) ;
#75310=EDGE_CURVE ( 'NONE', #65583, #11023, #98170, .T. ) ;
#75311=CARTESIAN_POINT ( 'NONE',  ( -87.62287095715005592, -23.72773821059535848, 11.05748984161097681 ) ) ;
#75312=CARTESIAN_POINT ( 'NONE',  ( -17.52035102510334141, -8.822347199899118309, 11.49999999999998934 ) ) ;
#75313=EDGE_CURVE ( 'NONE', #84333, #58299, #30799, .T. ) ;
#75314=DIRECTION ( 'NONE',  ( -3.773278334453079618E-23, 0.9999999999976377785, 2.173523156925979975E-06 ) ) ;
#75315=ORIENTED_EDGE ( 'NONE', *, *, #53740, .T. ) ;
#75317=CARTESIAN_POINT ( 'NONE',  ( 19.98928912078053699, -8.061568661392884749, -1.500000000000002220 ) ) ;
#75318=CARTESIAN_POINT ( 'NONE',  ( -33.60985848733059811, -23.73791477778911130, 11.05961554403171299 ) ) ;
#75320=CARTESIAN_POINT ( 'NONE',  ( -123.5895376238167245, -23.48786465467241769, 11.44779295918253759 ) ) ;
#75321=CARTESIAN_POINT ( 'NONE',  ( -50.52287095715006160, -23.47593901973090169, -1.443836447538997092 ) ) ;
#75322=CARTESIAN_POINT ( 'NONE',  ( -100.2462005486704442, -25.27473224266274343, 3.306208248721503651 ) ) ;
#75323=CARTESIAN_POINT ( 'NONE',  ( 3.160899137004691717, 22.77513019406404382, -1.500000000000002220 ) ) ;
#75325=DIRECTION ( 'NONE',  ( -3.773278334444167608E-23, 1.000000000000000000, 0.000000000000000000 ) ) ;
#75326=DIRECTION ( 'NONE',  ( -3.773278334453079030E-23, 0.9999999999976377785, 2.173523156925979128E-06 ) ) ;
#75327=CARTESIAN_POINT ( 'NONE',  ( -7.184633862932894743, 18.80532529184710100, 11.49999999999999645 ) ) ;
#75328=CARTESIAN_POINT ( 'NONE',  ( -45.62287095715006302, -24.82576562982390911, 8.398263435472966165 ) ) ;
#75329=DIRECTION ( 'NONE',  ( 0.000000000000000000, -2.173523156925980399E-06, 0.9999999999976378895 ) ) ;
#75330=CARTESIAN_POINT ( 'NONE',  ( -94.58953762381673869, -23.48786465467241769, 11.44779295918254114 ) ) ;
#75331=LINE ( 'NONE', #75828, #82907 ) ;
#75332=CARTESIAN_POINT ( 'NONE',  ( -111.3157468039189695, -25.29779307598838400, 3.994351246507165332 ) ) ;
#75333=CARTESIAN_POINT ( 'NONE',  ( -1.214729172165279092, -19.82145330704504360, 11.49999999999998934 ) ) ;
#75334=CARTESIAN_POINT ( 'NONE',  ( -51.52287095715006870, -29.50250786944525672, 11.44777988621624054 ) ) ;
#75335=CARTESIAN_POINT ( 'NONE',  ( 5.507670110241905448, 19.00313184189250038, -1.500000000000002220 ) ) ;
#75340=CARTESIAN_POINT ( 'NONE',  ( 18.97174343470660318, 8.267356841975738391, 11.49999999999999645 ) ) ;
#75341=CARTESIAN_POINT ( 'NONE',  ( -98.62287095715005592, -29.50250786944525672, 11.44777988621623166 ) ) ;
#75342=PLANE ( 'NONE',  #91802 ) ;
#75343=CARTESIAN_POINT ( 'NONE',  ( -78.62287095715005592, -29.50248528299804818, 1.056150453629038477 ) ) ;
#75344=CARTESIAN_POINT ( 'NONE',  ( -17.66434017299383896, 14.31182286555179139, 11.49999999999999645 ) ) ;
#75347=CARTESIAN_POINT ( 'NONE',  ( -42.52287095715005449, -23.47596703998600631, 11.44779298504229281 ) ) ;
#75348=B_SPLINE_CURVE_WITH_KNOTS ( 'NONE', 3,
 ( #11568, #42547, #3481, #3978, #51141, #28797, #83065, #75453 ),
 .UNSPECIFIED., .F., .F.,
 ( 4, 2, 2, 4 ),
 ( -0.001224554619866348448, -0.0002241820295893694366, 0.0007761905606876095751, 0.002776935741241576272 ),
 .UNSPECIFIED. ) ;
#75350=AXIS2_PLACEMENT_3D ( 'NONE', #90257, #97856, #59313 ) ;
#75353=AXIS2_PLACEMENT_3D ( 'NONE', #52053, #91598, #59170 ) ;
#75354=ORIENTED_EDGE ( 'NONE', *, *, #36022, .F. ) ;
#75356=CARTESIAN_POINT ( 'NONE',  ( -17.76840699843883442, -14.40508365592194195, -1.500000000000002220 ) ) ;
#75357=CARTESIAN_POINT ( 'NONE',  ( -29.58014010773451119, -24.43378003436859558, 0.6176547996449982536 ) ) ;
#75358=CARTESIAN_POINT ( 'NONE',  ( -16.60028029328060128, 13.79055755010687356, -1.500000000000002220 ) ) ;
#75359=CARTESIAN_POINT ( 'NONE',  ( -104.5228709571500758, -29.50247984919015209, -1.443849546365050029 ) ) ;
#75360=CARTESIAN_POINT ( 'NONE',  ( -103.5228709571501042, -23.47593901973090524, -1.443836447538996204 ) ) ;
#75361=CARTESIAN_POINT ( 'NONE',  ( 13.09772080625096891, 18.35129493929886380, 11.49999999999999645 ) ) ;
#75362=ORIENTED_EDGE ( 'NONE', *, *, #57358, .F. ) ;
#75364=CARTESIAN_POINT ( 'NONE',  ( 21.96865551644221881, -1.217672407684077918, 11.49999999999998934 ) ) ;
#75365=B_SPLINE_CURVE_WITH_KNOTS ( 'NONE', 3,
 ( #34127, #18392, #56974, #20372, #3680, #28006 ),
 .UNSPECIFIED., .F., .F.,
 ( 4, 2, 4 ),
 ( 6.391158118973929294E-06, 0.001387004593080789615, 0.002767618028042605031 ),
 .UNSPECIFIED. ) ;
#75367=CARTESIAN_POINT ( 'NONE',  ( -64.52287095715010423, -24.33832256527049154, 0.1851278514138605669 ) ) ;
#75368=CARTESIAN_POINT ( 'NONE',  ( -29.00356289826891754, -25.21724786265444607, 6.647730440730820867 ) ) ;
#75369=ORIENTED_EDGE ( 'NONE', *, *, #8188, .F. ) ;
#75372=CARTESIAN_POINT ( 'NONE',  ( -90.64148822836325792, -23.85049219812686161, 10.88485053497527488 ) ) ;
#75375=EDGE_LOOP ( 'NONE', ( #55415, #30274, #71824, #27080 ) ) ;
#75376=ORIENTED_EDGE ( 'NONE', *, *, #80746, .T. ) ;
#75378=CARTESIAN_POINT ( 'NONE',  ( -104.5228709571500758, -23.73907113216990084, -1.053371485793246354 ) ) ;
#75379=FACE_OUTER_BOUND ( 'NONE', #62330, .T. ) ;
#75380=CARTESIAN_POINT ( 'NONE',  ( -19.05221060042639536, -7.346018566486852031, -1.500000000000002220 ) ) ;
#75381=EDGE_CURVE ( 'NONE', #94475, #1915, #20712, .T. ) ;
#75384=CARTESIAN_POINT ( 'NONE',  ( -99.52287095715007581, -23.96177878511310055, 10.65340807706329507 ) ) ;
#75386=CARTESIAN_POINT ( 'NONE',  ( -47.52287095715006160, -23.48786465467240347, 11.44779295918255002 ) ) ;
#75387=ORIENTED_EDGE ( 'NONE', *, *, #9048, .T. ) ;
#75388=DIRECTION ( 'NONE',  ( -1.000000000000000000, -3.773278334444167608E-23, -8.201307833595939069E-29 ) ) ;
#75391=CARTESIAN_POINT ( 'NONE',  ( 11.01739540223112357, 17.63107602209319680, -1.500000000000002220 ) ) ;
#75392=EDGE_LOOP ( 'NONE', ( #74272, #43093, #76708, #9412 ) ) ;
#75395=ORIENTED_EDGE ( 'NONE', *, *, #19968, .F. ) ;
#75396=CARTESIAN_POINT ( 'NONE',  ( -68.52287095715010423, -23.95044443724990657, 10.65354141964648704 ) ) ;
#75398=VERTEX_POINT ( 'NONE', #98803 ) ;
#75399=LINE ( 'NONE', #15002, #78603 ) ;
#75403=CARTESIAN_POINT ( 'NONE',  ( 5.777647480883832287, 21.37485705712154171, 11.49999999999999645 ) ) ;
#75405=DIRECTION ( 'NONE',  ( -0.000000000000000000, 2.173523156925979552E-06, -0.9999999999976378895 ) ) ;
#75406=CARTESIAN_POINT ( 'NONE',  ( -6.441999407266626676, 21.70310835763521595, -1.500000000000002220 ) ) ;
#75407=CARTESIAN_POINT ( 'NONE',  ( -99.16166289166535819, -25.30166215957521914, 5.311370747606397380 ) ) ;
#75408=ORIENTED_EDGE ( 'NONE', *, *, #13599, .T. ) ;
#75409=B_SPLINE_CURVE_WITH_KNOTS ( 'NONE', 3,
 ( #53610, #39862, #30750, #802, #70822, #31753, #93638, #1312 ),
 .UNSPECIFIED., .F., .F.,
 ( 4, 2, 2, 4 ),
 ( -0.001224873891641427596, -0.0002244903592271119651, 0.0007758931731872036660, 0.002776660238015834711 ),
 .UNSPECIFIED. ) ;
#75411=LINE ( 'NONE', #36370, #66146 ) ;
#75414=CARTESIAN_POINT ( 'NONE',  ( -3.374260732160392795, -19.82512954709321562, 11.49999999999998934 ) ) ;
#75415=CARTESIAN_POINT ( 'NONE',  ( -105.6228709571500417, -29.50248789122583659, 2.256150453626215580 ) ) ;
#75416=VERTEX_POINT ( 'NONE', #31292 ) ;
#75418=CARTESIAN_POINT ( 'NONE',  ( -5.617636847906702258, 21.56867655435222630, -1.500000000000002220 ) ) ;
#75419=VECTOR ( 'NONE', #5057, 1000.000000000000114 ) ;
#75422=CARTESIAN_POINT ( 'NONE',  ( -95.52287095715004739, -23.47593901973090169, -1.443836447538996648 ) ) ;
#75424=LINE ( 'NONE', #41637, #13310 ) ;
#75426=CARTESIAN_POINT ( 'NONE',  ( -43.62287095715003460, -23.47596703998600276, 11.44779298504227505 ) ) ;
#75427=CARTESIAN_POINT ( 'NONE',  ( -1.081029368968937421, 19.50181592447522050, -1.500000000000002220 ) ) ;
#75428=EDGE_CURVE ( 'NONE', #57047, #49573, #46525, .T. ) ;
#75429=CARTESIAN_POINT ( 'NONE',  ( -14.42888051209446409, 15.91495273949476363, -1.500000000000002220 ) ) ;
#75431=EDGE_CURVE ( 'NONE', #2274, #38855, #34032, .T. ) ;
#75433=CARTESIAN_POINT ( 'NONE',  ( -115.6228709571500559, -24.99132157543166954, 2.256160258750667502 ) ) ;
#75434=CARTESIAN_POINT ( 'NONE',  ( -16.39533425382319720, 15.89506036719111037, -1.500000000000002220 ) ) ;
#75436=CARTESIAN_POINT ( 'NONE',  ( -96.62548630188759091, -24.51419770103159834, 9.386484678747169852 ) ) ;
#75438=CARTESIAN_POINT ( 'NONE',  ( -11.50144725928494438, 16.33591932373696665, 11.49999999999999645 ) ) ;
#75439=PLANE ( 'NONE',  #14442 ) ;
#75440=CARTESIAN_POINT ( 'NONE',  ( -35.62287095715005592, -23.48786465467240347, 11.44779295918255180 ) ) ;
#75446=CARTESIAN_POINT ( 'NONE',  ( -21.25272785503416273, -4.502612752106283978, 11.49999999999998934 ) ) ;
#75448=CARTESIAN_POINT ( 'NONE',  ( -5.392953615240748455, 18.82278424538476713, -1.500000000000002220 ) ) ;
#75449=CARTESIAN_POINT ( 'NONE',  ( -34.52287095715006870, -23.73907113217657283, -1.053371485781498196 ) ) ;
#75453=CARTESIAN_POINT ( 'NONE',  ( -60.62287095715005592, -23.48786465467241058, 11.44779295918254824 ) ) ;
#75454=CARTESIAN_POINT ( 'NONE',  ( -47.52287095715006160, -24.64965694238406613, 8.947790433994203596 ) ) ;
#75455=CARTESIAN_POINT ( 'NONE',  ( -20.18818894172909140, 3.697778396234267184, 11.49999999999999645 ) ) ;
#75456=CARTESIAN_POINT ( 'NONE',  ( -47.52287095715004739, -24.66019654487199375, 8.947790411086122830 ) ) ;
#75457=B_SPLINE_CURVE_WITH_KNOTS ( 'NONE', 3,
 ( #5792, #20507, #42878, #73809, #59100, #97151, #36747, #67715, #66227, #50988 ),
 .UNSPECIFIED., .F., .F.,
 ( 4, 2, 2, 2, 4 ),
 ( 0.000000000000000000, 0.0002022805416562973376, 0.0004045610833125946751, 0.0006068416249688920669, 0.0008091221666251893502 ),
 .UNSPECIFIED. ) ;
#75459=B_SPLINE_CURVE_WITH_KNOTS ( 'NONE', 3,
 ( #48207, #25354, #72543, #87252, #1529, #48718, #56331, #72049 ),
 .UNSPECIFIED., .F., .F.,
 ( 4, 2, 2, 4 ),
 ( -0.001240666984356058765, -0.0002401179793396618616, 0.0007604310256767346076, 0.002761529035709530365 ),
 .UNSPECIFIED. ) ;
#75462=CARTESIAN_POINT ( 'NONE',  ( -40.45829750704998418, -25.18430871329344356, 3.293943118056679165 ) ) ;
#75463=FACE_OUTER_BOUND ( 'NONE', #52578, .T. ) ;
#75465=ORIENTED_EDGE ( 'NONE', *, *, #91511, .T. ) ;
#75466=CARTESIAN_POINT ( 'NONE',  ( -119.6228709571500701, -24.51283580621365132, 0.6167428607019876940 ) ) ;
#75468=CARTESIAN_POINT ( 'NONE',  ( 12.94906671069258763, 19.00495796004926419, 11.49999999999999645 ) ) ;
#75469=CARTESIAN_POINT ( 'NONE',  ( -9.230423729802735622, -20.81519635545753033, 11.49999999999998934 ) ) ;
#75470=CARTESIAN_POINT ( 'NONE',  ( -106.6228709571500559, -29.50250243563736774, 8.947779886222136270 ) ) ;
#75473=LINE ( 'NONE', #67898, #12268 ) ;
#75474=CARTESIAN_POINT ( 'NONE',  ( -103.6228709571500417, -23.47596703998600631, 11.44779298504227860 ) ) ;
#75475=CARTESIAN_POINT ( 'NONE',  ( 12.66425630052701479, 17.85959152241435177, -1.500000000000002220 ) ) ;
#75482=CARTESIAN_POINT ( 'NONE',  ( -94.62287095715005592, -23.73934037231758154, 11.05740245334328442 ) ) ;
#75483=DIRECTION ( 'NONE',  ( -1.000000000000000000, -3.773278334444166432E-23, -8.201307841325785021E-29 ) ) ;
#75484=VERTEX_POINT ( 'NONE', #68367 ) ;
#75485=AXIS2_PLACEMENT_3D ( 'NONE', #39101, #31492, #7658 ) ;
#75486=CARTESIAN_POINT ( 'NONE',  ( 0.3735783541106268979, -20.45636175344465713, 11.49999999999998934 ) ) ;
#75490=VERTEX_POINT ( 'NONE', #99303 ) ;
#75491=ORIENTED_EDGE ( 'NONE', *, *, #51601, .F. ) ;
#75492=CARTESIAN_POINT ( 'NONE',  ( 22.88022663504679599, 2.825535151426334934, -1.500000000000002220 ) ) ;
#75493=DIRECTION ( 'NONE',  ( 0.000000000000000000, -2.173523156925980399E-06, 0.9999999999976378895 ) ) ;
#75494=CARTESIAN_POINT ( 'NONE',  ( -11.13811422090317294, 16.88724661786912762, -1.500000000000002220 ) ) ;
#75498=CARTESIAN_POINT ( 'NONE',  ( -42.52287095715005449, -24.64965694238575011, 8.947790433994205372 ) ) ;
#75499=VECTOR ( 'NONE', #55790, 1000.000000000000114 ) ;
#75500=B_SPLINE_CURVE_WITH_KNOTS ( 'NONE', 3,
 ( #73278, #3772, #67668, #42835 ),
 .UNSPECIFIED., .F., .F.,
 ( 4, 4 ),
 ( 1.583065275649749065E-09, 0.0004001880791969523793 ),
 .UNSPECIFIED. ) ;
#75502=CARTESIAN_POINT ( 'NONE',  ( -67.52287095715006160, -24.65952944569304961, 1.056160979905697239 ) ) ;
#75503=CARTESIAN_POINT ( 'NONE',  ( -7.526967427842778946, 20.06989004931119425, 11.49999999999999645 ) ) ;
#75504=VERTEX_POINT ( 'NONE', #53152 ) ;
#75505=FACE_OUTER_BOUND ( 'NONE', #59196, .T. ) ;
#75506=CARTESIAN_POINT ( 'NONE',  ( -41.57628542697372609, -24.65952944569304606, 1.056160979905696351 ) ) ;
#75507=EDGE_LOOP ( 'NONE', ( #21898, #61073, #28437, #90915 ) ) ;
#75508=CARTESIAN_POINT ( 'NONE',  ( -9.423985339279758122, -18.44656043379632848, -1.500000000000002220 ) ) ;
#75511=ORIENTED_EDGE ( 'NONE', *, *, #9192, .T. ) ;
#75516=CARTESIAN_POINT ( 'NONE',  ( -12.59924929152775874, 16.77720732749412846, -1.500000000000002220 ) ) ;
#75517=CARTESIAN_POINT ( 'NONE',  ( 17.58553779993395594, 13.13030503331179411, 11.49999999999999645 ) ) ;
#75518=CARTESIAN_POINT ( 'NONE',  ( -73.55905819736636886, -23.73791477778911840, 11.05961554403170766 ) ) ;
#75519=CARTESIAN_POINT ( 'NONE',  ( -11.58057713800463162, -19.31455136971746001, -1.500000000000002220 ) ) ;
#75520=ADVANCED_FACE ( 'NONE', ( #86580 ), #9459, .T. ) ;
#75522=CARTESIAN_POINT ( 'NONE',  ( -17.07941033872765146, 12.18221932706078370, -1.500000000000002220 ) ) ;
#75524=FACE_OUTER_BOUND ( 'NONE', #74602, .T. ) ;
#75525=CARTESIAN_POINT ( 'NONE',  ( -30.64643973578111158, -23.50395946778992240, -1.461890965025843814 ) ) ;
#75529=CARTESIAN_POINT ( 'NONE',  ( -128.6228709571500417, -23.48786465467242479, 11.44779295918253403 ) ) ;
#75530=CARTESIAN_POINT ( 'NONE',  ( 19.32660459246815421, -9.429101867163046435, -1.500000000000002220 ) ) ;
#75533=CARTESIAN_POINT ( 'NONE',  ( -8.144517828999388698, 19.50133175306300970, -1.500000000000002220 ) ) ;
#75534=CARTESIAN_POINT ( 'NONE',  ( -52.62287095715007723, -23.95044443724992078, 10.65354141964650125 ) ) ;
#75535=CARTESIAN_POINT ( 'NONE',  ( -81.88534077628074215, -25.24685308744633616, 6.293942982122114671 ) ) ;
#75536=CARTESIAN_POINT ( 'NONE',  ( -83.50334353477138905, -24.51419770103157347, 9.386484678747180510 ) ) ;
#75537=CARTESIAN_POINT ( 'NONE',  ( -33.52287095715006160, -24.66019654487198665, 8.947790411086131712 ) ) ;
#75538=CARTESIAN_POINT ( 'NONE',  ( -99.13348957873378708, -25.24983560723895692, 3.836871924205407680 ) ) ;
#75539=CARTESIAN_POINT ( 'NONE',  ( -10.67647856527443473, 19.39090429279614369, -1.500000000000002220 ) ) ;
#75540=CARTESIAN_POINT ( 'NONE',  ( -81.62637662810675465, -24.51419770103159834, 9.386484678747182286 ) ) ;
#75542=ORIENTED_EDGE ( 'NONE', *, *, #77185, .T. ) ;
#75544=DIRECTION ( 'NONE',  ( 0.000000000000000000, 0.9999999999976377785, 2.173523156925979975E-06 ) ) ;
#75546=CARTESIAN_POINT ( 'NONE',  ( -100.5497506620879165, -24.52300882791530512, 0.6510814631126384810 ) ) ;
#75547=CARTESIAN_POINT ( 'NONE',  ( -19.39930850525863804, 0.8904154686948315689, 11.49999999999998934 ) ) ;
#75548=CARTESIAN_POINT ( 'NONE',  ( -2.881439591185620319, 21.19155266312798958, -1.500000000000002220 ) ) ;
#75549=CARTESIAN_POINT ( 'NONE',  ( -73.62287095715005592, -24.64965695001468404, 8.947790433994184056 ) ) ;
#75554=B_SPLINE_CURVE_WITH_KNOTS ( 'NONE', 3,
 ( #64583, #26989, #11260, #94992 ),
 .UNSPECIFIED., .F., .F.,
 ( 4, 4 ),
 ( 0.000000000000000000, 9.999999999999592548E-05 ),
 .UNSPECIFIED. ) ;
#75555=CARTESIAN_POINT ( 'NONE',  ( -22.51868310087907687, -2.221351303042197411, -1.500000000000002220 ) ) ;
#75556=AXIS2_PLACEMENT_3D ( 'NONE', #1255, #8350, #47422 ) ;
#75560=CARTESIAN_POINT ( 'NONE',  ( -41.52287095715006870, -23.47596703998600631, 11.44779298504229281 ) ) ;
#75561=CARTESIAN_POINT ( 'NONE',  ( 18.46520180437041603, 7.126043738416648843, 11.49999999999999645 ) ) ;
#75562=CARTESIAN_POINT ( 'NONE',  ( -74.52287095715007581, -23.48783264082476308, -1.443836473390090802 ) ) ;
#75568=CARTESIAN_POINT ( 'NONE',  ( -87.55620429048339304, -23.47596703998600631, 11.44779298504227683 ) ) ;
#75569=CARTESIAN_POINT ( 'NONE',  ( 13.31326451270642330, 17.06472021985377552, 11.49999999999998934 ) ) ;
#75571=CARTESIAN_POINT ( 'NONE',  ( 7.147005326088517130, -18.03964237587283037, -1.500000000000002220 ) ) ;
#75573=CARTESIAN_POINT ( 'NONE',  ( -61.62287095715004881, -24.51283580621364777, 0.6167428607019832532 ) ) ;
#75575=CARTESIAN_POINT ( 'NONE',  ( 16.85830656838225039, -10.38424343889589707, -1.500000000000002220 ) ) ;
#75576=ORIENTED_EDGE ( 'NONE', *, *, #50356, .T. ) ;
#75577=CARTESIAN_POINT ( 'NONE',  ( 20.12614038868121824, 2.982395457389826809, 11.49999999999999645 ) ) ;
#75578=CARTESIAN_POINT ( 'NONE',  ( -101.6228709571500559, -29.50250243563736774, 8.947779886222138046 ) ) ;
#75581=CARTESIAN_POINT ( 'NONE',  ( -30.64427850938830389, -23.56000036390796382, -1.497999999999532150 ) ) ;
#75582=CARTESIAN_POINT ( 'NONE',  ( -111.5122638532038337, -25.29712067403331233, 4.332404411321261861 ) ) ;
#75583=CARTESIAN_POINT ( 'NONE',  ( -99.58953762381672448, -23.48786465467241769, 11.44779295918254114 ) ) ;
#75584=CARTESIAN_POINT ( 'NONE',  ( -82.52287095715006160, -23.48786465467241058, 11.44779295918254469 ) ) ;
#75586=CARTESIAN_POINT ( 'NONE',  ( -1.723993941171178879, -19.98520929721398431, 11.49999999999998934 ) ) ;
#75587=CARTESIAN_POINT ( 'NONE',  ( -95.55620429048340725, -24.99132157543166954, 2.256160258750667946 ) ) ;
#75589=CARTESIAN_POINT ( 'NONE',  ( -117.6228709571500701, -24.50321055353806088, 9.387540953477516936 ) ) ;
#75590=VECTOR ( 'NONE', #73169, 1000.000000000000114 ) ;
#75591=CARTESIAN_POINT ( 'NONE',  ( 4.181975289622855918, -22.47981636197143374, 11.49999999999999645 ) ) ;
#75592=CARTESIAN_POINT ( 'NONE',  ( -30.47287095715008931, -25.29726141536321293, 4.434337432396732837 ) ) ;
#75594=LINE ( 'NONE', #6097, #50066 ) ;
#75596=DIRECTION ( 'NONE',  ( -1.000000000000000000, -3.773278334444167608E-23, -8.201307833595939069E-29 ) ) ;
#75597=ADVANCED_FACE ( 'NONE', ( #10454 ), #25177, .F. ) ;
#75599=ORIENTED_EDGE ( 'NONE', *, *, #46036, .F. ) ;
#75600=CARTESIAN_POINT ( 'NONE',  ( -18.95781532540867076, -7.450117396690965066, -1.500000000000002220 ) ) ;
#75601=EDGE_LOOP ( 'NONE', ( #5367, #16614, #13664, #95157 ) ) ;
#75602=CARTESIAN_POINT ( 'NONE',  ( 16.23347398924790497, -16.23827457187686463, -1.500000000000002220 ) ) ;
#75605=CARTESIAN_POINT ( 'NONE',  ( -101.5468792378191978, -25.24282061761980955, 6.236250683194342059 ) ) ;
#75608=B_SPLINE_CURVE_WITH_KNOTS ( 'NONE', 3,
 ( #16647, #15649, #46618, #78032 ),
 .UNSPECIFIED., .F., .F.,
 ( 4, 4 ),
 ( 0.5001430643975933732, 0.5091494956697090180 ),
 .UNSPECIFIED. ) ;
#75609=CARTESIAN_POINT ( 'NONE',  ( -86.62287095715004170, -24.65952944569304606, 1.056160979905700348 ) ) ;
#75610=CARTESIAN_POINT ( 'NONE',  ( 10.81949470224598997, -18.29866561848832518, 11.49999999999999645 ) ) ;
#75612=ORIENTED_EDGE ( 'NONE', *, *, #95148, .T. ) ;
#75613=CARTESIAN_POINT ( 'NONE',  ( 19.86420646539740176, -9.926203236129387264, 11.49999999999998934 ) ) ;
#75614=CARTESIAN_POINT ( 'NONE',  ( -20.60669311552257810, 0.8253496925510150906, -1.500000000000002220 ) ) ;
#75617=B_SPLINE_CURVE_WITH_KNOTS ( 'NONE', 3,
 ( #73279, #88003, #18482, #34712, #94606, #3282 ),
 .UNSPECIFIED., .F., .F.,
 ( 4, 2, 4 ),
 ( 0.000000000000000000, 0.001380764517854761930, 0.002761529035709523860 ),
 .UNSPECIFIED. ) ;
#75618=ORIENTED_EDGE ( 'NONE', *, *, #13274, .F. ) ;
#75622=ORIENTED_EDGE ( 'NONE', *, *, #64838, .F. ) ;
#75624=VECTOR ( 'NONE', #95619, 1000.000000000000227 ) ;
#75625=AXIS2_PLACEMENT_3D ( 'NONE', #61579, #53962, #80793 ) ;
#75626=ORIENTED_EDGE ( 'NONE', *, *, #74744, .F. ) ;
#75628=CARTESIAN_POINT ( 'NONE',  ( -111.5172617135973354, -24.15620529776629510, 10.23563542870659582 ) ) ;
#75630=CARTESIAN_POINT ( 'NONE',  ( 16.93201058511109380, 12.15574511561022852, -1.500000000000002220 ) ) ;
#75631=CARTESIAN_POINT ( 'NONE',  ( 16.38291735060997567, -14.39268585342195905, 11.49999999999999645 ) ) ;
#75632=CARTESIAN_POINT ( 'NONE',  ( -51.16262983862578295, -25.06317656708942820, 7.418605103709588811 ) ) ;
#75633=CARTESIAN_POINT ( 'NONE',  ( -52.52287095715009002, -24.33832256527048088, 0.1851278514138577636 ) ) ;
#75634=CARTESIAN_POINT ( 'NONE',  ( 11.36419782745769069, 19.35538867594532775, -1.500000000000002220 ) ) ;
#75640=CARTESIAN_POINT ( 'NONE',  ( -75.52287095715009002, -24.82558206586143967, 1.605769216559449930 ) ) ;
#75641=CARTESIAN_POINT ( 'NONE',  ( -50.38191529551148307, -25.11033443737753146, 2.832404817301930056 ) ) ;
#75645=FACE_OUTER_BOUND ( 'NONE', #67038, .T. ) ;
#75646=ORIENTED_EDGE ( 'NONE', *, *, #82231, .T. ) ;
#75647=CARTESIAN_POINT ( 'NONE',  ( -18.72683625574626376, -10.08736549105613278, -1.500000000000002220 ) ) ;
#75648=EDGE_LOOP ( 'NONE', ( #49900, #89149, #37718, #94473 ) ) ;
#75650=CARTESIAN_POINT ( 'NONE',  ( -2.129267666952235682, 20.92775224702969439, 11.49999999999998934 ) ) ;
#75651=CARTESIAN_POINT ( 'NONE',  ( -55.62287095715004170, -23.47596703998600631, 11.44779298504227505 ) ) ;
#75652=CARTESIAN_POINT ( 'NONE',  ( -100.4326965455115044, -25.18492896333868103, 3.293943116708551777 ) ) ;
#75653=FACE_OUTER_BOUND ( 'NONE', #57683, .T. ) ;
#75654=CARTESIAN_POINT ( 'NONE',  ( -17.33335002049248530, 13.43749923854009509, -1.500000000000002220 ) ) ;
#75655=CARTESIAN_POINT ( 'NONE',  ( -87.55830571644068527, -23.73766607897671932, -1.055555164236430032 ) ) ;
#75656=VERTEX_POINT ( 'NONE', #59018 ) ;
#75657=CARTESIAN_POINT ( 'NONE',  ( -122.6263441853496943, -23.73791477778912551, 11.05961554403169878 ) ) ;
#75660=CARTESIAN_POINT ( 'NONE',  ( -120.5228709571500758, -23.84047902841604483, -0.8780736468305403442 ) ) ;
#75661=CARTESIAN_POINT ( 'NONE',  ( -39.52287095715008292, -23.48783264082476308, -1.443836473390098574 ) ) ;
#75663=CARTESIAN_POINT ( 'NONE',  ( -30.61243602696747956, -24.47944986445295612, 9.440663514584128890 ) ) ;
#75664=CARTESIAN_POINT ( 'NONE',  ( -13.45305159987462851, 16.49040971879131234, -1.500000000000002220 ) ) ;
#75665=CARTESIAN_POINT ( 'NONE',  ( -47.62287095715004881, -24.66019654487199020, 8.947790411086133489 ) ) ;
#75666=CARTESIAN_POINT ( 'NONE',  ( -107.6339985510269059, -23.48786465467241413, 11.44779295918253759 ) ) ;
#75668=CARTESIAN_POINT ( 'NONE',  ( -29.62287096154833677, -23.39681786206389447, 11.44779298504227860 ) ) ;
#75669=CARTESIAN_POINT ( 'NONE',  ( -33.51256534245839447, -23.73766607897670866, -1.055555164236444687 ) ) ;
#75670=CARTESIAN_POINT ( 'NONE',  ( -9.984083066403742990, 20.14924292131567185, -1.500000000000002220 ) ) ;
#75671=B_SPLINE_SURFACE_WITH_KNOTS ( 'NONE', 3, 1, ( 
 ( #35155, #64632 ),
 ( #41266, #4201 ),
 ( #57003, #34158 ),
 ( #33143, #17421 ),
 ( #40759, #10811 ),
 ( #2712, #42775 ),
 ( #88441, #72219 ),
 ( #18914, #26030 ),
 ( #96048, #73708 ),
 ( #17927, #66126 ),
 ( #81321, #79313 ),
 ( #26542, #2214 ),
 ( #87938, #95546 ),
 ( #11802, #48884 ),
 ( #3221, #86928 ),
 ( #49893, #9808 ),
 ( #33652, #25028 ),
 ( #56002, #64126 ),
 ( #79812, #18422 ) ),
 .UNSPECIFIED., .F., .F., .F.,
 ( 4, 1, 1, 1, 1, 1, 1, 1, 1, 1, 1, 1, 1, 1, 1, 1, 4 ),
 ( 2, 2 ),
 ( 0.000000000000000000, 0.06542114375888925804, 0.1287083718818818057, 0.1902361418635387103, 0.2507244020335389068, 0.3106371794134432096, 0.3707664082897241253, 0.4316147444123512589, 0.4935229735663542727, 0.5558834553775323650, 0.6173423673185097771, 0.6786680390972755772, 0.7407113595451459975, 0.8029853625127446604, 0.8668025802655175971, 0.9323471713458875154, 1.000000000000000000 ),
 ( 0.000000000000000000, 1.000000000000000000 ),
 .UNSPECIFIED. ) ;
#75673=CARTESIAN_POINT ( 'NONE',  ( -57.52287095715008292, -23.47593901973090524, -1.443836447538997092 ) ) ;
#75674=ORIENTED_EDGE ( 'NONE', *, *, #52862, .F. ) ;
#75676=CARTESIAN_POINT ( 'NONE',  ( -15.21066300689680872, 12.40131300380995860, 11.49999999999999645 ) ) ;
#75677=CARTESIAN_POINT ( 'NONE',  ( -78.52287095715004739, -24.66019654487199375, 8.947790411086119278 ) ) ;
#75678=CARTESIAN_POINT ( 'NONE',  ( -82.52287095715000476, -24.34917612407037524, 0.1852690917478629073 ) ) ;
#75679=EDGE_LOOP ( 'NONE', ( #61169, #45249, #69416, #82274 ) ) ;
#75681=CARTESIAN_POINT ( 'NONE',  ( -88.54822851708769349, -24.35071581493543746, 9.817618358456025263 ) ) ;
#75682=CARTESIAN_POINT ( 'NONE',  ( -108.6228709571500417, -24.66019654487199730, 8.947790411086124607 ) ) ;
#75683=CARTESIAN_POINT ( 'NONE',  ( -99.38203303823797796, -25.25095903933959463, 5.782495831883606385 ) ) ;
#75685=CARTESIAN_POINT ( 'NONE',  ( -26.36060433830035876, -24.68582954907684268, 7.705587838995554328 ) ) ;
#75687=CARTESIAN_POINT ( 'NONE',  ( -16.88869819569221065, 10.18974688345344148, -1.500000000000002220 ) ) ;
#75688=EDGE_CURVE ( 'NONE', #31325, #83369, #5966, .T. ) ;
#75689=ORIENTED_EDGE ( 'NONE', *, *, #29834, .T. ) ;
#75690=LINE ( 'NONE', #59999, #47235 ) ;
#75695=CARTESIAN_POINT ( 'NONE',  ( -124.5228709571500616, -23.47596703998600631, 11.44779298504227860 ) ) ;
#75699=CARTESIAN_POINT ( 'NONE',  ( -45.58953762381671737, -24.99156044556202261, 7.747789690856172307 ) ) ;
#75701=CARTESIAN_POINT ( 'NONE',  ( -119.5228709571500758, -23.47596703998600631, 11.44779298504227860 ) ) ;
#75702=CARTESIAN_POINT ( 'NONE',  ( -120.5562042904833930, -23.47593901973091235, -1.443836447538997536 ) ) ;
#75703=CARTESIAN_POINT ( 'NONE',  ( 19.86680303116296287, 2.261939200664708327, -1.500000000000002220 ) ) ;
#75704=CARTESIAN_POINT ( 'NONE',  ( -125.6228709571500275, -24.92604778743017846, 8.074972756849355449 ) ) ;
#75705=CARTESIAN_POINT ( 'NONE',  ( -89.40841769935767047, -29.50249691823240994, 6.409318347766594037 ) ) ;
#75708=CARTESIAN_POINT ( 'NONE',  ( -107.5228709571501042, -23.47593901973090524, -1.443836447538996426 ) ) ;
#75709=CARTESIAN_POINT ( 'NONE',  ( -80.55273171905794527, -24.15602025860895807, 10.28564288303536145 ) ) ;
#75710=CARTESIAN_POINT ( 'NONE',  ( -49.62287095715005592, -23.73934037231756733, 11.05740245334328975 ) ) ;
#75711=CARTESIAN_POINT ( 'NONE',  ( -81.50567729269914707, -24.34968618360933945, 0.1864209137778954084 ) ) ;
#75712=CARTESIAN_POINT ( 'NONE',  ( -27.75512989467660674, -24.60093890593964261, 1.629583950786930968 ) ) ;
#75713=CARTESIAN_POINT ( 'NONE',  ( -45.52287095715007581, -25.00182538069144655, 7.747789668545101094 ) ) ;
#75715=CARTESIAN_POINT ( 'NONE',  ( -127.5212392067688540, -24.34968618360935011, 0.1864209137778923830 ) ) ;
#75716=ORIENTED_EDGE ( 'NONE', *, *, #70416, .T. ) ;
#75717=CARTESIAN_POINT ( 'NONE',  ( -11.05657426389776354, 17.00066307926000420, 11.49999999999998934 ) ) ;
#75718=CARTESIAN_POINT ( 'NONE',  ( -70.18583440245234328, -25.31468095713259103, 4.854010836220668423 ) ) ;
#75723=DIRECTION ( 'NONE',  ( -1.000000000000000000, -3.773278334444167608E-23, -8.201307833595939069E-29 ) ) ;
#75724=CARTESIAN_POINT ( 'NONE',  ( -51.62287095715005592, -29.50248528299804818, 1.056150453629033370 ) ) ;
#75725=CARTESIAN_POINT ( 'NONE',  ( -12.53166870608491479, 15.75175023352509385, -1.500000000000002220 ) ) ;
#75726=CARTESIAN_POINT ( 'NONE',  ( 9.660767377612277329, -18.76748907076374095, 11.49999999999999645 ) ) ;
#75730=CARTESIAN_POINT ( 'NONE',  ( -70.56769529849768219, -23.48786465467241058, 11.44779295918254824 ) ) ;
#75731=CARTESIAN_POINT ( 'NONE',  ( -20.36895902721504825, -8.506870616244709637, -1.500000000000002220 ) ) ;
#75732=CARTESIAN_POINT ( 'NONE',  ( -4.863915844574979275, 19.94883092034378791, 11.49999999999998934 ) ) ;
#75733=CARTESIAN_POINT ( 'NONE',  ( -35.55620429048339304, -24.99132157543166244, 2.256160258750668390 ) ) ;
#75736=VERTEX_POINT ( 'NONE', #30497 ) ;
#75738=ORIENTED_EDGE ( 'NONE', *, *, #70764, .F. ) ;
#75740=CARTESIAN_POINT ( 'NONE',  ( -129.6228709571500417, -23.47596703998600631, 11.44779298504227683 ) ) ;
#75741=EDGE_CURVE ( 'NONE', #75171, #53102, #48, .T. ) ;
#75742=EDGE_LOOP ( 'NONE', ( #40836, #55471, #53432, #66106 ) ) ;
#75747=CARTESIAN_POINT ( 'NONE',  ( 19.36870410414886479, 7.000668502413378569, -1.500000000000002220 ) ) ;
#75749=CARTESIAN_POINT ( 'NONE',  ( -2.376235263977734657, 21.45616117177731041, 11.49999999999999645 ) ) ;
#75751=CARTESIAN_POINT ( 'NONE',  ( -70.74026866089612042, -25.30511070033976395, 4.894904393956083233 ) ) ;
#75753=CARTESIAN_POINT ( 'NONE',  ( -7.140196579304709523, 21.16591527347414115, -1.500000000000002220 ) ) ;
#75754=EDGE_CURVE ( 'NONE', #23443, #46454, #43544, .T. ) ;
#75756=EDGE_CURVE ( 'NONE', #9193, #49692, #13763, .T. ) ;
#75757=CARTESIAN_POINT ( 'NONE',  ( -74.62287095715005592, -29.50248528299804818, 1.056150453629036701 ) ) ;
#75758=DIRECTION ( 'NONE',  ( -3.773278334453079030E-23, 0.9999999999976377785, 2.173523156925979128E-06 ) ) ;
#75760=DIRECTION ( 'NONE',  ( 0.000000000000000000, 2.173523156925980399E-06, -0.9999999999976378895 ) ) ;
#75763=CARTESIAN_POINT ( 'NONE',  ( 19.40856703110355852, -7.758221025823637262, -1.500000000000002220 ) ) ;
#75765=CARTESIAN_POINT ( 'NONE',  ( -86.50206692487462590, -24.65952944569304961, 1.056160979905701680 ) ) ;
#75766=ORIENTED_EDGE ( 'NONE', *, *, #69276, .F. ) ;
#75768=CARTESIAN_POINT ( 'NONE',  ( -100.5908655779713712, -24.40133493613050319, 9.663955038902802386 ) ) ;
#75769=CARTESIAN_POINT ( 'NONE',  ( 6.139388171429570384, 20.22809724653347985, -1.500000000000002220 ) ) ;
#75771=CARTESIAN_POINT ( 'NONE',  ( -117.5527649515685340, -24.51314013834316086, 0.6176544820404215042 ) ) ;
#75772=CARTESIAN_POINT ( 'NONE',  ( -96.62287095715005592, -29.50247984919015209, -1.443849546365050029 ) ) ;
#75773=CARTESIAN_POINT ( 'NONE',  ( -3.523925741820590929, 21.50064390955241578, -1.500000000000002220 ) ) ;
#75776=CARTESIAN_POINT ( 'NONE',  ( -76.55889698137454502, -23.73791477778911840, 11.05961554403170766 ) ) ;
#75777=LINE ( 'NONE', #6276, #23811 ) ;
#75778=CARTESIAN_POINT ( 'NONE',  ( -20.93004649427559016, -6.003493321846349318, -1.500000000000002220 ) ) ;
#75779=CARTESIAN_POINT ( 'NONE',  ( -71.64734380851882634, -25.31639660058803543, 5.762066634805036003 ) ) ;
#75780=CARTESIAN_POINT ( 'NONE',  ( 4.697571063781373013, 21.84268702631108994, 11.49999999999999645 ) ) ;
#75781=ORIENTED_EDGE ( 'NONE', *, *, #5547, .T. ) ;
#75782=CARTESIAN_POINT ( 'NONE',  ( -55.62287095715005592, -23.47593901973091235, -1.443836447539007972 ) ) ;
#75784=EDGE_CURVE ( 'NONE', #51543, #42958, #29994, .T. ) ;
#75786=ORIENTED_EDGE ( 'NONE', *, *, #49450, .T. ) ;
#75787=B_SPLINE_CURVE_WITH_KNOTS ( 'NONE', 3,
 ( #49965, #65696, #97117, #41338 ),
 .UNSPECIFIED., .F., .F.,
 ( 4, 4 ),
 ( 0.000000000000000000, 9.999999999999592548E-05 ),
 .UNSPECIFIED. ) ;
#75789=EDGE_CURVE ( 'NONE', #85381, #99016, #59363, .T. ) ;
#75792=CARTESIAN_POINT ( 'NONE',  ( 16.79009078985406234, 12.93418496121567252, -1.500000000000002220 ) ) ;
#75793=FACE_OUTER_BOUND ( 'NONE', #18399, .T. ) ;
#75794=CARTESIAN_POINT ( 'NONE',  ( 8.286623624103266097E-13, -23.05000000000000426, -1.500000000000002220 ) ) ;
#75795=EDGE_CURVE ( 'NONE', #73004, #95213, #65323, .T. ) ;
#75796=CARTESIAN_POINT ( 'NONE',  ( -124.5228709571500616, -24.64898659630368627, 1.056161002820833028 ) ) ;
#75798=CARTESIAN_POINT ( 'NONE',  ( -14.46832242630667942, -12.86894606327920876, 11.49999999999998934 ) ) ;
#75799=CARTESIAN_POINT ( 'NONE',  ( -38.52287095715006870, -24.50216790748204332, 0.6166512839542463986 ) ) ;
#75800=ORIENTED_EDGE ( 'NONE', *, *, #80073, .F. ) ;
#75801=CARTESIAN_POINT ( 'NONE',  ( -3.206006181753352724, -19.19236486397402430, 11.49999999999999645 ) ) ;
#75802=CARTESIAN_POINT ( 'NONE',  ( -69.52287095715006160, -24.33832256527049154, 0.1851278514138574860 ) ) ;
#75803=EDGE_LOOP ( 'NONE', ( #11604, #5291, #67019, #99945 ) ) ;
#75805=DIRECTION ( 'NONE',  ( -3.773278334444167608E-23, 1.000000000000000000, 0.000000000000000000 ) ) ;
#75808=CARTESIAN_POINT ( 'NONE',  ( -30.64427850938831099, -23.47596703998600276, 11.44779298504227683 ) ) ;
#75810=CARTESIAN_POINT ( 'NONE',  ( -14.21210043416151159, 13.53504130633199765, -1.500000000000002220 ) ) ;
#75812=CARTESIAN_POINT ( 'NONE',  ( -33.62287095715005592, -23.48786465467240347, 11.44779295918255535 ) ) ;
#75813=EDGE_LOOP ( 'NONE', ( #4742, #33519, #48222, #85989 ) ) ;
#75814=CARTESIAN_POINT ( 'NONE',  ( -10.34410514300256523, -18.92461576200269491, -1.500000000000002220 ) ) ;
#75817=DIRECTION ( 'NONE',  ( 0.000000000000000000, -0.9999999999976377785, -2.173523156925979975E-06 ) ) ;
#75818=EDGE_CURVE ( 'NONE', #1680, #94949, #21773, .T. ) ;
#75819=CARTESIAN_POINT ( 'NONE',  ( -100.4326965455115044, -25.18439335745797436, 3.293943117872703663 ) ) ;
#75820=CARTESIAN_POINT ( 'NONE',  ( -22.55714481399219906, -4.634528848986672500, -1.500000000000002220 ) ) ;
#75823=CARTESIAN_POINT ( 'NONE',  ( -88.62287095715004170, -23.47596703998600631, 11.44779298504227860 ) ) ;
#75824=CARTESIAN_POINT ( 'NONE',  ( 11.25103634530202790, -16.72154935384561725, 11.49999999999999645 ) ) ;
#75825=CARTESIAN_POINT ( 'NONE',  ( -84.62287095715008434, -23.95044443724992789, 10.65354141964649592 ) ) ;
#75828=CARTESIAN_POINT ( 'NONE',  ( -118.6228709571500559, -29.50250786944525672, 11.44777988621622811 ) ) ;
#75829=B_SPLINE_CURVE_WITH_KNOTS ( 'NONE', 3,
 ( #1114, #40176, #2127, #85845, #39663, #107 ),
 .UNSPECIFIED., .F., .F.,
 ( 4, 2, 4 ),
 ( 1.570887131794638196E-05, 0.001396322306279761073, 0.002776935741241575838 ),
 .UNSPECIFIED. ) ;
#75830=CARTESIAN_POINT ( 'NONE',  ( -110.9011049686103263, -25.18425615697176667, 3.445933459401032906 ) ) ;
#75831=EDGE_CURVE ( 'NONE', #28831, #803, #84686, .T. ) ;
#75832=CARTESIAN_POINT ( 'NONE',  ( 14.69432462292611952, 13.40460087117274490, -1.500000000000002220 ) ) ;
#75834=CARTESIAN_POINT ( 'NONE',  ( -15.39140670439391378, -12.39996395878027791, -1.500000000000002220 ) ) ;
#75839=CARTESIAN_POINT ( 'NONE',  ( 12.98984941077313415, -16.12360325096057423, 11.49999999999999645 ) ) ;
#75840=CARTESIAN_POINT ( 'NONE',  ( -128.5562042904834357, -24.64965694238575722, 8.947790433994187609 ) ) ;
#75841=AXIS2_PLACEMENT_3D ( 'NONE', #24473, #91985, #7748 ) ;
#75843=CARTESIAN_POINT ( 'NONE',  ( -79.58953762381672448, -23.47596703998600276, 11.44779298504227683 ) ) ;
#75844=B_SPLINE_CURVE_WITH_KNOTS ( 'NONE', 3,
 ( #27864, #16000, #99239, #76397 ),
 .UNSPECIFIED., .F., .F.,
 ( 4, 4 ),
 ( 0.000000000000000000, 1.000000000000000000 ),
 .UNSPECIFIED. ) ;
#75845=CARTESIAN_POINT ( 'NONE',  ( 0.6941480231959694658, 22.73124288027050710, 11.49999999999999645 ) ) ;
#75846=ORIENTED_EDGE ( 'NONE', *, *, #43975, .T. ) ;
#75847=CARTESIAN_POINT ( 'NONE',  ( -78.58953762381671027, -24.65952944569304606, 1.056160979905698571 ) ) ;
#75849=CARTESIAN_POINT ( 'NONE',  ( 9.409760114191467295, 17.86087837679851020, 11.49999999999998934 ) ) ;
#75850=CARTESIAN_POINT ( 'NONE',  ( -63.49151771392492805, -24.65952944569304250, 1.056160979905695463 ) ) ;
#75851=DIRECTION ( 'NONE',  ( -3.773278334444167608E-23, 1.000000000000000000, 0.000000000000000000 ) ) ;
#75852=EDGE_LOOP ( 'NONE', ( #68439, #92565, #61045, #44923 ) ) ;
#75853=ORIENTED_EDGE ( 'NONE', *, *, #62652, .F. ) ;
#75855=CARTESIAN_POINT ( 'NONE',  ( 1.119804705421552748, 22.86502198858056545, 11.49999999999998934 ) ) ;
#75856=CARTESIAN_POINT ( 'NONE',  ( -111.3631985155635249, -25.27898041276672814, 4.195814472291353070 ) ) ;
#75857=CARTESIAN_POINT ( 'NONE',  ( 17.62533924669398999, -12.40915598911231577, -1.500000000000002220 ) ) ;
#75859=CARTESIAN_POINT ( 'NONE',  ( -123.5563712463038115, -23.73766607897670866, -1.055555164236449350 ) ) ;
#75860=CARTESIAN_POINT ( 'NONE',  ( -34.53827696482609610, -24.34968618360933590, 0.1864209137778841396 ) ) ;
#75861=CARTESIAN_POINT ( 'NONE',  ( 20.36350155627077640, -4.707376482769925374, 11.49999999999999645 ) ) ;
#75863=CARTESIAN_POINT ( 'NONE',  ( -43.52287095715004739, -23.48783264083374078, -1.443836473376152840 ) ) ;
#75864=B_SPLINE_CURVE_WITH_KNOTS ( 'NONE', 3,
 ( #61291, #91216, #22190, #30824, #29320, #28827, #68883, #36933, #60292, #75981, #52664, #5984, #83095, #59792 ),
 .UNSPECIFIED., .F., .F.,
 ( 4, 2, 2, 2, 2, 2, 4 ),
 ( 6.992893892674702526E-18, 0.0001898996604258977995, 0.0003797993208517886059, 0.0007595986417035701646, 0.001139397962555351723, 0.001329297622981238762, 0.001519197283407126018 ),
 .UNSPECIFIED. ) ;
#75865=CARTESIAN_POINT ( 'NONE',  ( -17.28599015371049674, 13.57978550619682956, -1.500000000000002220 ) ) ;
#75866=CARTESIAN_POINT ( 'NONE',  ( -105.6281865643600497, -24.52399227489126687, 9.353111116836517525 ) ) ;
#75867=CARTESIAN_POINT ( 'NONE',  ( -29.05583327267715532, -24.79700080848643040, 6.516963030855588812 ) ) ;
#75868=VERTEX_POINT ( 'NONE', #38614 ) ;
#75871=PLANE ( 'NONE',  #75353 ) ;
#75873=FACE_OUTER_BOUND ( 'NONE', #6890, .T. ) ;
#75874=ADVANCED_FACE ( 'NONE', ( #63989 ), #16777, .T. ) ;
#75875=ORIENTED_EDGE ( 'NONE', *, *, #7994, .F. ) ;
#75876=ADVANCED_FACE ( 'NONE', ( #8674 ), #46738, .F. ) ;
#75877=ORIENTED_EDGE ( 'NONE', *, *, #63427, .F. ) ;
#75878=CARTESIAN_POINT ( 'NONE',  ( -106.6228709571501128, -23.73907113216991860, -1.053371485793221929 ) ) ;
#75881=CARTESIAN_POINT ( 'NONE',  ( 14.85214116200856083, 13.97194181870810326, -1.500000000000002220 ) ) ;
#75886=EDGE_CURVE ( 'NONE', #49859, #66424, #2399, .T. ) ;
#75888=CARTESIAN_POINT ( 'NONE',  ( -25.67463369986340993, -24.84696307844978946, 6.403790676681452965 ) ) ;
#75889=ORIENTED_EDGE ( 'NONE', *, *, #25894, .F. ) ;
#75890=DIRECTION ( 'NONE',  ( 1.000000000000000000, 3.773278334444166432E-23, 8.201307841325785021E-29 ) ) ;
#75891=CARTESIAN_POINT ( 'NONE',  ( -28.79021057664958505, -24.63645989546533954, 7.906029157777645366 ) ) ;
#75892=CARTESIAN_POINT ( 'NONE',  ( 14.74948264216024008, 14.65492983226340407, 11.49999999999998934 ) ) ;
#75897=CARTESIAN_POINT ( 'NONE',  ( -68.52287095715006160, -24.64965694238407323, 8.947790433994200043 ) ) ;
#75898=ORIENTED_EDGE ( 'NONE', *, *, #57077, .F. ) ;
#75899=ORIENTED_EDGE ( 'NONE', *, *, #24017, .F. ) ;
#75903=CARTESIAN_POINT ( 'NONE',  ( -106.6228709571500559, -29.50248528299804818, 1.056150453629043584 ) ) ;
#75904=CARTESIAN_POINT ( 'NONE',  ( -92.54896780759155206, -24.35071581493542681, 9.817618358456023486 ) ) ;
#75905=CARTESIAN_POINT ( 'NONE',  ( -95.62287095715005592, -23.47596703998600631, 11.44779298504227860 ) ) ;
#75906=CARTESIAN_POINT ( 'NONE',  ( 4.116201370682176730, 21.75534844777131838, 11.49999999999999645 ) ) ;
#75909=CARTESIAN_POINT ( 'NONE',  ( -9.675873947287982446, 20.46574270456686406, -1.500000000000002220 ) ) ;
#75911=CARTESIAN_POINT ( 'NONE',  ( -27.97447329329273558, -24.82855238255122998, 7.574514681721855602 ) ) ;
#75912=ORIENTED_EDGE ( 'NONE', *, *, #68908, .F. ) ;
#75915=CARTESIAN_POINT ( 'NONE',  ( -8.609638109768802394, 18.19638482192696216, -1.500000000000002220 ) ) ;
#75918=VECTOR ( 'NONE', #16445, 1000.000000000000114 ) ;
#75919=CARTESIAN_POINT ( 'NONE',  ( -103.6228709571500559, -24.64965695001469115, 8.947790433994178727 ) ) ;
#75920=CARTESIAN_POINT ( 'NONE',  ( 12.52526618502215250, 18.50471055633022388, -1.500000000000002220 ) ) ;
#75921=ORIENTED_EDGE ( 'NONE', *, *, #39676, .T. ) ;
#75924=FACE_OUTER_BOUND ( 'NONE', #23093, .T. ) ;
#75926=EDGE_CURVE ( 'NONE', #11110, #100229, #71582, .T. ) ;
#75927=CARTESIAN_POINT ( 'NONE',  ( -96.62287095715015539, -24.35013146730205236, 9.818937971375108376 ) ) ;
#75929=CARTESIAN_POINT ( 'NONE',  ( 12.07855387261060898, -15.37489856218140183, 11.49999999999998934 ) ) ;
#75930=AXIS2_PLACEMENT_3D ( 'NONE', #104, #39159, #70116 ) ;
#75931=CARTESIAN_POINT ( 'NONE',  ( -85.62287095715005592, -29.50248528299804818, 1.056150453629040253 ) ) ;
#75932=CARTESIAN_POINT ( 'NONE',  ( -10.41973078503355588, 18.78793304046337198, 11.49999999999998934 ) ) ;
#75933=CARTESIAN_POINT ( 'NONE',  ( -25.68905881183481199, -24.92775057940327343, 3.430378144321810208 ) ) ;
#75937=CARTESIAN_POINT ( 'NONE',  ( -12.24191887126339751, 19.33842681661653984, -1.500000000000002220 ) ) ;
#75939=LINE ( 'NONE', #35412, #93650 ) ;
#75940=CARTESIAN_POINT ( 'NONE',  ( -91.52287095715006160, -23.48786465467241769, 11.44779295918254292 ) ) ;
#75941=CARTESIAN_POINT ( 'NONE',  ( -19.59816365915598979, -3.832847594873297403, 11.49999999999999645 ) ) ;
#75942=CARTESIAN_POINT ( 'NONE',  ( -64.62287095715005592, -24.64898659630528499, 1.056161002820822592 ) ) ;
#75943=B_SPLINE_CURVE_WITH_KNOTS ( 'NONE', 3,
 ( #69128, #15330, #25340, #76719 ),
 .UNSPECIFIED., .F., .F.,
 ( 4, 4 ),
 ( 0.000000000000000000, 9.999999999998897304E-05 ),
 .UNSPECIFIED. ) ;
#75944=CARTESIAN_POINT ( 'NONE',  ( -74.63458368284264566, -24.15620529776628800, 10.23563542870659937 ) ) ;
#75946=ORIENTED_EDGE ( 'NONE', *, *, #91723, .F. ) ;
#75947=DIRECTION ( 'NONE',  ( 0.000000000000000000, -0.9999999999976377785, -2.173523156925979975E-06 ) ) ;
#75949=CARTESIAN_POINT ( 'NONE',  ( -21.72135255055207281, 0.4632500610043824851, 11.49999999999998934 ) ) ;
#75950=LINE ( 'NONE', #60755, #15574 ) ;
#75951=CARTESIAN_POINT ( 'NONE',  ( -16.13938233076020268, 11.07636124087057183, -1.500000000000002220 ) ) ;
#75952=PLANE ( 'NONE',  #32906 ) ;
#75953=ORIENTED_EDGE ( 'NONE', *, *, #23117, .F. ) ;
#75956=CARTESIAN_POINT ( 'NONE',  ( -71.70841769935766763, -25.25720466352798255, 6.192981421160952848 ) ) ;
#75957=CARTESIAN_POINT ( 'NONE',  ( -1.317410511717131971, -20.46822056820986546, 11.49999999999999645 ) ) ;
#75959=B_SPLINE_CURVE_WITH_KNOTS ( 'NONE', 3,
 ( #66101, #97017, #65101, #56478, #88414, #96515 ),
 .UNSPECIFIED., .F., .F.,
 ( 4, 2, 4 ),
 ( 1.570755371633875854E-05, 0.001396183895866087970, 0.002776660238015836880 ),
 .UNSPECIFIED. ) ;
#75962=LINE ( 'NONE', #59771, #70250 ) ;
#75964=CARTESIAN_POINT ( 'NONE',  ( -116.5222327913904934, -23.48786465467241769, 11.44779295918253759 ) ) ;
#75966=LINE ( 'NONE', #59776, #37039 ) ;
#75967=CARTESIAN_POINT ( 'NONE',  ( -124.6228709571499991, -24.51387760970725083, 9.387446482453405849 ) ) ;
#75970=CARTESIAN_POINT ( 'NONE',  ( 21.63105218614105851, 7.968772182826888262, 11.49999999999999645 ) ) ;
#75971=CARTESIAN_POINT ( 'NONE',  ( 12.37853024107498534, -19.16169124346054176, -1.500000000000002220 ) ) ;
#75972=FACE_OUTER_BOUND ( 'NONE', #43455, .T. ) ;
#75974=CARTESIAN_POINT ( 'NONE',  ( -49.54611987101804971, -25.25386647804926099, 3.777482285138224150 ) ) ;
#75975=VECTOR ( 'NONE', #13069, 1000.000000000000114 ) ;
#75976=CARTESIAN_POINT ( 'NONE',  ( -115.5228709571501611, -24.92579138211019796, 1.929029949965660684 ) ) ;
#75977=CARTESIAN_POINT ( 'NONE',  ( -99.37735140507533060, -25.30157721269421955, 5.086082750430767518 ) ) ;
#75978=CARTESIAN_POINT ( 'NONE',  ( -0.1377007522546883911, -21.91379463844567965, 11.49999999999998934 ) ) ;
#75981=CARTESIAN_POINT ( 'NONE',  ( -41.40626431004942276, -25.30540310050566077, 4.501526219705256793 ) ) ;
#75982=CARTESIAN_POINT ( 'NONE',  ( -58.52287095715006160, -24.64898659630528499, 1.056161002820822592 ) ) ;
#75983=CARTESIAN_POINT ( 'NONE',  ( -112.6228709571500417, -23.72747288104441665, -1.053458166803660889 ) ) ;
#75984=CARTESIAN_POINT ( 'NONE',  ( -122.6228709571500417, -23.48786465467242124, 11.44779295918253759 ) ) ;
#75985=VERTEX_POINT ( 'NONE', #40123 ) ;
#75986=EDGE_CURVE ( 'NONE', #68982, #82055, #88298, .T. ) ;
#75988=CARTESIAN_POINT ( 'NONE',  ( 20.35601985306173134, -1.938729116259007679, -1.500000000000002220 ) ) ;
#75991=ORIENTED_EDGE ( 'NONE', *, *, #77257, .T. ) ;
#75993=CARTESIAN_POINT ( 'NONE',  ( 3.314627170985911420, 22.80399709308638023, -1.500000000000002220 ) ) ;
#75994=FACE_OUTER_BOUND ( 'NONE', #76187, .T. ) ;
#75995=CARTESIAN_POINT ( 'NONE',  ( -17.27845874757997535, -10.49745931960568335, -1.500000000000002220 ) ) ;
#75996=ADVANCED_FACE ( 'NONE', ( #54353 ), #1571, .F. ) ;
#75997=ORIENTED_EDGE ( 'NONE', *, *, #83318, .F. ) ;
#75998=CARTESIAN_POINT ( 'NONE',  ( -48.52287095715004028, -23.95044443724991723, 10.65354141964649237 ) ) ;
#75999=CARTESIAN_POINT ( 'NONE',  ( -46.52287095715006160, -24.64898659630367561, 1.056161002820821038 ) ) ;
#76002=DIRECTION ( 'NONE',  ( 0.000000000000000000, -0.9999999999976377785, -2.173523156925979975E-06 ) ) ;
#76003=CARTESIAN_POINT ( 'NONE',  ( -19.04320821261859464, -9.809917703373946196, 11.49999999999999645 ) ) ;
#76006=B_SPLINE_CURVE_WITH_KNOTS ( 'NONE', 3,
 ( #59403, #91841, #37059, #38056, #21320, #44183 ),
 .UNSPECIFIED., .F., .F.,
 ( 4, 2, 4 ),
 ( 6.391158118958419274E-06, 0.001387004593080778557, 0.002767618028042598960 ),
 .UNSPECIFIED. ) ;
#76007=CARTESIAN_POINT ( 'NONE',  ( -61.62365995700092469, -24.66019654487199375, 8.947790411086119278 ) ) ;
#76010=EDGE_CURVE ( 'NONE', #66631, #39813, #98262, .T. ) ;
#76011=CARTESIAN_POINT ( 'NONE',  ( -9.423985339279758122, -18.44656043379632848, 11.49999999999998934 ) ) ;
#76012=CARTESIAN_POINT ( 'NONE',  ( -70.30743997983631743, -25.24386760754551418, 3.513016081743164598 ) ) ;
#76014=ORIENTED_EDGE ( 'NONE', *, *, #46036, .T. ) ;
#76015=CARTESIAN_POINT ( 'NONE',  ( -91.52287095715006160, -23.48786465467241769, 11.44779295918254292 ) ) ;
#76016=ORIENTED_EDGE ( 'NONE', *, *, #67007, .T. ) ;
#76020=CARTESIAN_POINT ( 'NONE',  ( 19.17116566557315949, -10.70166234769870961, 11.49999999999999645 ) ) ;
#76021=CARTESIAN_POINT ( 'NONE',  ( -37.60092905518352069, -23.96169478059712432, 10.65365249895718591 ) ) ;
#76022=CARTESIAN_POINT ( 'NONE',  ( 19.88857169258762170, 10.62688394266798930, -1.500000000000002220 ) ) ;
#76023=CARTESIAN_POINT ( 'NONE',  ( -15.18370147500227496, -14.46048895944246127, 11.49999999999998934 ) ) ;
#76028=ORIENTED_EDGE ( 'NONE', *, *, #92041, .F. ) ;
#76029=ORIENTED_EDGE ( 'NONE', *, *, #45791, .F. ) ;
#76030=CARTESIAN_POINT ( 'NONE',  ( -66.56566039321768358, -23.48783264082476308, -1.443836473390097463 ) ) ;
#76031=CARTESIAN_POINT ( 'NONE',  ( 11.78165356204951131, -17.99452314462042324, -1.500000000000002220 ) ) ;
#76032=CARTESIAN_POINT ( 'NONE',  ( -105.5228709571500900, -23.84081130425358097, 10.88220057483157888 ) ) ;
#76033=EDGE_LOOP ( 'NONE', ( #38591, #26093, #79033, #49959 ) ) ;
#76034=CARTESIAN_POINT ( 'NONE',  ( -9.089321149825819290, -19.05894737874082168, -1.500000000000002220 ) ) ;
#76035=CARTESIAN_POINT ( 'NONE',  ( -83.55620429048340725, -24.64898659630529210, 1.056161002820828809 ) ) ;
#76037=VECTOR ( 'NONE', #58650, 1000.000000000000114 ) ;
#76038=CARTESIAN_POINT ( 'NONE',  ( -100.5228709571500900, -23.48783264082477018, -1.443836473390086583 ) ) ;
#76040=CARTESIAN_POINT ( 'NONE',  ( -42.22287095715005734, -23.47593901973090169, -1.443836447538997980 ) ) ;
#76041=CARTESIAN_POINT ( 'NONE',  ( -0.8124730928778809425, -22.15030348749839817, -1.500000000000002220 ) ) ;
#76043=B_SPLINE_CURVE_WITH_KNOTS ( 'NONE', 3,
 ( #72601, #12175, #19290, #95427 ),
 .UNSPECIFIED., .F., .F.,
 ( 4, 4 ),
 ( 0.000000000000000000, 1.000000000000000000 ),
 .UNSPECIFIED. ) ;
#76044=EDGE_CURVE ( 'NONE', #99009, #21700, #75424, .T. ) ;
#76050=EDGE_CURVE ( 'NONE', #41368, #46438, #41213, .T. ) ;
#76051=PLANE ( 'NONE',  #28500 ) ;
#76053=CARTESIAN_POINT ( 'NONE',  ( 12.19879910451502703, -15.15100395215988449, 11.49999999999998934 ) ) ;
#76054=VECTOR ( 'NONE', #58295, 1000.000000000000227 ) ;
#76055=CARTESIAN_POINT ( 'NONE',  ( 20.74164082462262471, 5.259929546262127609, -1.500000000000002220 ) ) ;
#76056=CARTESIAN_POINT ( 'NONE',  ( -62.50954302324786482, -23.96119346886881019, -0.6495511937832096905 ) ) ;
#76057=FACE_OUTER_BOUND ( 'NONE', #72681, .T. ) ;
#76058=B_SPLINE_CURVE_WITH_KNOTS ( 'NONE', 3,
 ( #9602, #34442, #63413, #63919, #19200, #3004 ),
 .UNSPECIFIED., .F., .F.,
 ( 4, 2, 4 ),
 ( 0.000000000000000000, 0.001380901958385387027, 0.002761803916770774053 ),
 .UNSPECIFIED. ) ;
#76059=EDGE_CURVE ( 'NONE', #6656, #25133, #3075, .T. ) ;
#76060=CARTESIAN_POINT ( 'NONE',  ( -79.62287095715004170, -24.65952944569304606, 1.056160979905697461 ) ) ;
#76061=FACE_OUTER_BOUND ( 'NONE', #52045, .T. ) ;
#76062=CARTESIAN_POINT ( 'NONE',  ( 16.66146196086182130, -15.28366505690825328, -1.500000000000002220 ) ) ;
#76064=ORIENTED_EDGE ( 'NONE', *, *, #65149, .T. ) ;
#76067=CARTESIAN_POINT ( 'NONE',  ( -40.62287095715005592, -23.47596703998600276, 11.44779298504227505 ) ) ;
#76068=CARTESIAN_POINT ( 'NONE',  ( 19.51516567812286596, -3.327523070855789911, 11.49999999999999645 ) ) ;
#76072=CARTESIAN_POINT ( 'NONE',  ( -32.62287095715005592, -24.66019654487199020, 8.947790411086137041 ) ) ;
#76073=CARTESIAN_POINT ( 'NONE',  ( 10.55456386191721663, 18.89434267519128596, -1.500000000000002220 ) ) ;
#76074=CARTESIAN_POINT ( 'NONE',  ( -26.95875550904777285, -24.78998600965948640, 7.383661286321142825 ) ) ;
#76075=CARTESIAN_POINT ( 'NONE',  ( 3.148799746435844593, 19.17640706095922098, -1.500000000000002220 ) ) ;
#76076=CARTESIAN_POINT ( 'NONE',  ( -80.52287095715007581, -24.52323809116984421, 9.355190652339421931 ) ) ;
#76077=LINE ( 'NONE', #21287, #36078 ) ;
#76078=CARTESIAN_POINT ( 'NONE',  ( -2.602694502683683631, -19.63732897141692391, -1.500000000000002220 ) ) ;
#76080=CARTESIAN_POINT ( 'NONE',  ( -20.32193514540556123, 0.06534614623005505218, 11.49999999999999645 ) ) ;
#76081=CARTESIAN_POINT ( 'NONE',  ( -111.5562042904833788, -24.66019654487199730, 8.947790411086124607 ) ) ;
#76083=CARTESIAN_POINT ( 'NONE',  ( -60.52287095715007581, -25.00182538069855198, 7.747789668514453609 ) ) ;
#76086=CARTESIAN_POINT ( 'NONE',  ( -0.06447947376607357506, -22.21526254151202551, 0.5319095616429412310 ) ) ;
#76087=CARTESIAN_POINT ( 'NONE',  ( -95.52287095715004739, -24.91570333825769978, 8.075032458260361423 ) ) ;
#76088=CARTESIAN_POINT ( 'NONE',  ( -49.35191700208513765, -25.31601870270916521, 5.185240284718970472 ) ) ;
#76090=CARTESIAN_POINT ( 'NONE',  ( -51.06408614287066428, -25.14734643380794310, 6.959314159085416840 ) ) ;
#76091=CARTESIAN_POINT ( 'NONE',  ( -11.36185547594953249, 16.55520930037988592, -1.500000000000002220 ) ) ;
#76092=DIRECTION ( 'NONE',  ( 0.000000000000000000, 0.9999999999976377785, 2.173523156925979128E-06 ) ) ;
#76094=CARTESIAN_POINT ( 'NONE',  ( -36.52287095715006870, -24.50216790748205398, 0.6166512839542417357 ) ) ;
#76095=CARTESIAN_POINT ( 'NONE',  ( -9.150087108448493822, 20.98025145036519845, 11.49999999999999645 ) ) ;
#76099=CARTESIAN_POINT ( 'NONE',  ( -71.55620429048337883, -24.64898659630528854, 1.056161002820825701 ) ) ;
#76102=B_SPLINE_CURVE_WITH_KNOTS ( 'NONE', 3,
 ( #2226, #9309, #64139, #12189, #10322, #4099 ),
 .UNSPECIFIED., .F., .F.,
 ( 4, 2, 4 ),
 ( 1.570887131794333942E-05, 0.001396322306279758904, 0.002776935741241574537 ),
 .UNSPECIFIED. ) ;
#76103=CARTESIAN_POINT ( 'NONE',  ( -111.5562042904834072, -23.47596703998600631, 11.44779298504227683 ) ) ;
#76105=CARTESIAN_POINT ( 'NONE',  ( -9.871001836803966256, -17.81128643866572148, -1.500000000000002220 ) ) ;
#76106=VERTEX_POINT ( 'NONE', #5428 ) ;
#76108=CARTESIAN_POINT ( 'NONE',  ( 9.743704349311032686, 20.77413290702584092, 11.49999999999998934 ) ) ;
#76109=FACE_OUTER_BOUND ( 'NONE', #34620, .T. ) ;
#76110=ORIENTED_EDGE ( 'NONE', *, *, #21239, .T. ) ;
#76111=AXIS2_PLACEMENT_3D ( 'NONE', #2683, #3682, #87403 ) ;
#76115=CARTESIAN_POINT ( 'NONE',  ( 8.286623624103266097E-13, -23.05000000000000426, -1.500000000000002220 ) ) ;
#76116=CARTESIAN_POINT ( 'NONE',  ( -18.64022381217131397, 10.26305532446727753, 11.49999999999999645 ) ) ;
#76117=ORIENTED_EDGE ( 'NONE', *, *, #83908, .T. ) ;
#76118=ADVANCED_FACE ( 'NONE', ( #87800 ), #95906, .F. ) ;
#76119=VECTOR ( 'NONE', #79359, 1000.000000000000114 ) ;
#76121=CARTESIAN_POINT ( 'NONE',  ( 21.18294168759468832, 6.642818831845659133, -1.500000000000002220 ) ) ;
#76122=ADVANCED_FACE ( 'NONE', ( #10675 ), #18286, .T. ) ;
#76123=CARTESIAN_POINT ( 'NONE',  ( 9.220172233967117492, 18.46515239161685784, -1.500000000000002220 ) ) ;
#76130=VERTEX_POINT ( 'NONE', #88302 ) ;
#76131=CARTESIAN_POINT ( 'NONE',  ( -127.2834285841887834, -25.28334328158019417, 4.245358510314064304 ) ) ;
#76133=CARTESIAN_POINT ( 'NONE',  ( 19.16185898538474675, 8.078635803559651052, -1.500000000000002220 ) ) ;
#76134=EDGE_CURVE ( 'NONE', #100298, #7254, #36364, .T. ) ;
#76135=CARTESIAN_POINT ( 'NONE',  ( 19.23208339725441007, -10.27600428404867827, 11.49999999999999645 ) ) ;
#76136=CARTESIAN_POINT ( 'NONE',  ( -51.93008262322722857, -25.24431853135508774, 6.222446891247057188 ) ) ;
#76137=CARTESIAN_POINT ( 'NONE',  ( -78.50133211539314004, -24.51419770103157347, 9.386484678747175181 ) ) ;
#76138=CARTESIAN_POINT ( 'NONE',  ( -3.368041826647835357, -22.21310627845187824, 11.49999999999998934 ) ) ;
#76139=CARTESIAN_POINT ( 'NONE',  ( -51.26061221361337061, -25.31296648395201032, 4.199398687311516554 ) ) ;
#76141=CARTESIAN_POINT ( 'NONE',  ( -50.52287095715007581, -25.00182538069144655, 7.747789668545104647 ) ) ;
#76142=CARTESIAN_POINT ( 'NONE',  ( -69.52287095715010423, -23.95044443724993144, 10.65354141964649237 ) ) ;
#76146=CARTESIAN_POINT ( 'NONE',  ( -46.64649981546305924, -23.96169478059712432, 10.65365249895718414 ) ) ;
#76147=ORIENTED_EDGE ( 'NONE', *, *, #98132, .T. ) ;
#76148=CARTESIAN_POINT ( 'NONE',  ( -4.607724273132460802, 20.83226218841027944, -1.500000000000002220 ) ) ;
#76149=ORIENTED_EDGE ( 'NONE', *, *, #65149, .F. ) ;
#76151=CARTESIAN_POINT ( 'NONE',  ( -11.62490142266122639, -17.50836435561060256, 11.49999999999998934 ) ) ;
#76152=CARTESIAN_POINT ( 'NONE',  ( -126.6228709571500559, -29.50248528299804818, 1.056150453629047137 ) ) ;
#76153=CARTESIAN_POINT ( 'NONE',  ( -99.74425588205387783, -25.21639837048163457, 3.531259653993959802 ) ) ;
#76154=CARTESIAN_POINT ( 'NONE',  ( -65.52287095715006160, -24.99156044556202616, 7.747789690856173195 ) ) ;
#76155=CARTESIAN_POINT ( 'NONE',  ( -21.09739860443290382, 5.981408608369527258, -1.500000000000002220 ) ) ;
#76156=FACE_OUTER_BOUND ( 'NONE', #52555, .T. ) ;
#76157=ORIENTED_EDGE ( 'NONE', *, *, #51988, .F. ) ;
#76158=CARTESIAN_POINT ( 'NONE',  ( -122.5222492067709368, -23.48786465467241769, 11.44779295918253581 ) ) ;
#76159=EDGE_CURVE ( 'NONE', #93802, #21835, #35100, .T. ) ;
#76160=EDGE_CURVE ( 'NONE', #49308, #70398, #77915, .T. ) ;
#76163=CARTESIAN_POINT ( 'NONE',  ( -10.27973282203687688, -22.47507199546397416, 10.47594215909544957 ) ) ;
#76164=CARTESIAN_POINT ( 'NONE',  ( 21.14028111218437900, -2.610574537768086234, -1.500000000000002220 ) ) ;
#76165=CARTESIAN_POINT ( 'NONE',  ( -98.58489322720483017, -24.66019654487200086, 8.947790411086119278 ) ) ;
#76166=CARTESIAN_POINT ( 'NONE',  ( -51.92287095715006018, -23.47596703998600631, 11.44779298504227683 ) ) ;
#76169=CARTESIAN_POINT ( 'NONE',  ( -90.62287095715011276, -24.62226745350440282, 0.9660975649728149595 ) ) ;
#76170=CARTESIAN_POINT ( 'NONE',  ( -33.57507691967732200, -24.65952944569304606, 1.056160979905695907 ) ) ;
#76171=CARTESIAN_POINT ( 'NONE',  ( 22.01961411883556252, 4.383451955130949429, -1.500000000000002220 ) ) ;
#76173=FACE_OUTER_BOUND ( 'NONE', #24724, .T. ) ;
#76174=ORIENTED_EDGE ( 'NONE', *, *, #38024, .T. ) ;
#76175=CARTESIAN_POINT ( 'NONE',  ( -81.52287095715001897, -24.66019654487199375, 8.947790411086126383 ) ) ;
#76176=CARTESIAN_POINT ( 'NONE',  ( 14.10018531369908423, 13.67006465538575277, 11.49999999999999645 ) ) ;
#76177=CARTESIAN_POINT ( 'NONE',  ( -68.62287095715005592, -23.47593901973091235, -1.443836447539006196 ) ) ;
#76179=DIRECTION ( 'NONE',  ( -3.773278334453079030E-23, 0.9999999999976377785, 2.173523156925979128E-06 ) ) ;
#76180=VERTEX_POINT ( 'NONE', #46992 ) ;
#76181=CARTESIAN_POINT ( 'NONE',  ( -121.5228709571500048, -23.47593901973090524, -1.443836447538996204 ) ) ;
#76182=FACE_OUTER_BOUND ( 'NONE', #50237, .T. ) ;
#76183=CARTESIAN_POINT ( 'NONE',  ( -100.1102081092206930, -25.25095791289925629, 5.264240324507090563 ) ) ;
#76184=CARTESIAN_POINT ( 'NONE',  ( -25.85390067486408583, -24.79634013197061648, 6.939180248999893053 ) ) ;
#76185=CARTESIAN_POINT ( 'NONE',  ( -19.50520112914412252, -2.896358124273927359, -1.500000000000002220 ) ) ;
#76186=VECTOR ( 'NONE', #48626, 1000.000000000000114 ) ;
#76187=EDGE_LOOP ( 'NONE', ( #10476, #56701, #56900, #64913 ) ) ;
#76189=CARTESIAN_POINT ( 'NONE',  ( -108.5895376238167245, -23.47596703998600631, 11.44779298504227683 ) ) ;
#76191=ADVANCED_FACE ( 'NONE', ( #91159 ), #69323, .F. ) ;
#76196=VECTOR ( 'NONE', #18588, 1000.000000000000114 ) ;
#76198=CARTESIAN_POINT ( 'NONE',  ( -55.48854651988001763, -24.63355581998386157, 0.9682620441943822209 ) ) ;
#76202=CARTESIAN_POINT ( 'NONE',  ( -70.32437837831572836, -25.31201590703328463, 5.314180722553312641 ) ) ;
#76203=CARTESIAN_POINT ( 'NONE',  ( -107.5162164984105004, -24.15543982623908192, -0.2315651400026443874 ) ) ;
#76204=CARTESIAN_POINT ( 'NONE',  ( -18.20579941527595480, -8.200869797747142087, 11.49999999999998934 ) ) ;
#76205=LINE ( 'NONE', #37655, #98517 ) ;
#76206=CARTESIAN_POINT ( 'NONE',  ( -45.53828599902652741, -24.52399227489127043, 9.353111116836528183 ) ) ;
#76209=EDGE_CURVE ( 'NONE', #77370, #85031, #39375, .T. ) ;
#76210=CARTESIAN_POINT ( 'NONE',  ( -119.6264739001214821, -23.96119346886881019, -0.6495511937832016969 ) ) ;
#76211=CARTESIAN_POINT ( 'NONE',  ( -80.58318537203670928, -24.83644354573579349, 8.397322867130101898 ) ) ;
#76212=CARTESIAN_POINT ( 'NONE',  ( -127.2832169593331741, -25.28351172706441830, 5.756926109542241043 ) ) ;
#76213=CARTESIAN_POINT ( 'NONE',  ( -39.58693056125937915, -24.34968618360933235, 0.1864209137778788383 ) ) ;
#76214=CARTESIAN_POINT ( 'NONE',  ( -27.85310647731327904, -25.26026286786085961, 1.631227119663390068 ) ) ;
#76217=CARTESIAN_POINT ( 'NONE',  ( -47.62287095715004881, -29.50248528299804818, 1.056150453629033370 ) ) ;
#76219=CARTESIAN_POINT ( 'NONE',  ( -20.02346298389695534, -3.155783441878276196, -1.500000000000002220 ) ) ;
#76221=CARTESIAN_POINT ( 'NONE',  ( -72.52287095715007581, -29.50248528299804818, 1.056150453629036701 ) ) ;
#76223=CARTESIAN_POINT ( 'NONE',  ( -99.62287095715004170, -24.50216790748097750, 0.6166512839513834665 ) ) ;
#76224=VERTEX_POINT ( 'NONE', #62227 ) ;
#76225=CARTESIAN_POINT ( 'NONE',  ( -60.52287095715006160, -29.50248789122583659, 2.256150453626215580 ) ) ;
#76226=CARTESIAN_POINT ( 'NONE',  ( -63.62287095715004881, -24.50216790748097395, 0.6166512839513691446 ) ) ;
#76227=CARTESIAN_POINT ( 'NONE',  ( -15.79248070760165490, 12.47733877207048181, -1.500000000000002220 ) ) ;
#76228=CARTESIAN_POINT ( 'NONE',  ( -18.71117167593497399, 9.704403692310313190, 11.49999999999999645 ) ) ;
#76230=CARTESIAN_POINT ( 'NONE',  ( 21.00647827173414939, 6.864759178008983831, -1.500000000000002220 ) ) ;
#76231=AXIS2_PLACEMENT_3D ( 'NONE', #39208, #22965, #38711 ) ;
#76233=CARTESIAN_POINT ( 'NONE',  ( -19.38928925021375349, 6.733644070511561885, 11.49999999999998934 ) ) ;
#76234=CARTESIAN_POINT ( 'NONE',  ( -66.62287095715005592, -24.66019654487199020, 8.947790411086131712 ) ) ;
#76235=CARTESIAN_POINT ( 'NONE',  ( -53.62287095715006302, -24.34917612406836795, 0.1852690917426561001 ) ) ;
#76238=VERTEX_POINT ( 'NONE', #85541 ) ;
#76240=DIRECTION ( 'NONE',  ( -3.773278334453080206E-23, 0.9999999999976377785, 2.173523156925979975E-06 ) ) ;
#76241=CARTESIAN_POINT ( 'NONE',  ( -29.62287095715004881, -23.39678932012542845, -1.443836140311830940 ) ) ;
#76242=EDGE_LOOP ( 'NONE', ( #39687, #97062, #27737, #37978 ) ) ;
#76245=CARTESIAN_POINT ( 'NONE',  ( -63.62287095715003460, -23.73907113216990794, -1.053371485793231699 ) ) ;
#76246=CARTESIAN_POINT ( 'NONE',  ( -68.60259347313552780, -23.73791477778911840, 11.05961554403170943 ) ) ;
#76247=CARTESIAN_POINT ( 'NONE',  ( -11.82494684808912844, 16.90534455221803967, -1.500000000000002220 ) ) ;
#76248=EDGE_CURVE ( 'NONE', #16861, #62297, #99267, .T. ) ;
#76249=CARTESIAN_POINT ( 'NONE',  ( 2.319523670979641849, -21.48760272935114557, 11.49999999999999645 ) ) ;
#76251=DIRECTION ( 'NONE',  ( 1.000000000000000000, 3.773278334444167608E-23, 8.201307833595939069E-29 ) ) ;
#76253=CARTESIAN_POINT ( 'NONE',  ( -2.124831620219566730, 22.23837930986240607, 11.49999999999998934 ) ) ;
#76255=CARTESIAN_POINT ( 'NONE',  ( -79.76746806413464697, -25.12205757671817352, 6.852562942996416773 ) ) ;
#76256=CARTESIAN_POINT ( 'NONE',  ( -84.56294249096249871, -23.48783264082476308, -1.443836473390094799 ) ) ;
#76257=VERTEX_POINT ( 'NONE', #32759 ) ;
#76258=DIRECTION ( 'NONE',  ( -3.773278334453079618E-23, 0.9999999999976377785, 2.173523156925979975E-06 ) ) ;
#76260=CARTESIAN_POINT ( 'NONE',  ( -49.61441931870202637, -23.48786465467241058, 11.44779295918254824 ) ) ;
#76262=CARTESIAN_POINT ( 'NONE',  ( -7.158894406585330827, 19.61798520005962487, 11.49999999999998934 ) ) ;
#76263=ORIENTED_EDGE ( 'NONE', *, *, #6221, .F. ) ;
#76264=CARTESIAN_POINT ( 'NONE',  ( -86.59170088307759272, -24.15543982623907482, -0.2315651400026493556 ) ) ;
#76267=CARTESIAN_POINT ( 'NONE',  ( -96.62287095715005592, -23.47593901973091235, -1.443836447539001089 ) ) ;
#76268=CARTESIAN_POINT ( 'NONE',  ( -13.58512445790048417, 16.25115196636789250, -1.500000000000002220 ) ) ;
#76269=VERTEX_POINT ( 'NONE', #18533 ) ;
#76271=CARTESIAN_POINT ( 'NONE',  ( -99.69221343823950576, -25.12215628115585631, 6.884718414011108401 ) ) ;
#76272=CARTESIAN_POINT ( 'NONE',  ( 21.79142754302170815, -0.6654467836950721527, 11.49999999999998934 ) ) ;
#76273=CARTESIAN_POINT ( 'NONE',  ( -129.6228709571500701, -23.48786465467241769, 11.44779295918253581 ) ) ;
#76274=CARTESIAN_POINT ( 'NONE',  ( -81.55620429048339304, -24.64898659630528854, 1.056161002820828143 ) ) ;
#76275=CARTESIAN_POINT ( 'NONE',  ( -33.22287095715005734, -23.47593901973090169, -1.443836447538998202 ) ) ;
#76276=CARTESIAN_POINT ( 'NONE',  ( -20.56741719582323213, 7.008553436993695485, -1.500000000000002220 ) ) ;
#76278=CARTESIAN_POINT ( 'NONE',  ( -12.45998644600372884, -18.51849504856558681, 11.49999999999999645 ) ) ;
#76280=PLANE ( 'NONE',  #82643 ) ;
#76283=ORIENTED_EDGE ( 'NONE', *, *, #55442, .T. ) ;
#76284=ORIENTED_EDGE ( 'NONE', *, *, #4204, .T. ) ;
#76285=ADVANCED_FACE ( 'NONE', ( #79932 ), #33767, .F. ) ;
#76287=CARTESIAN_POINT ( 'NONE',  ( -85.58953762381672448, -23.48786465467241413, 11.44779295918254114 ) ) ;
#76288=CARTESIAN_POINT ( 'NONE',  ( -14.68016216564755894, -15.32010671487267572, -1.500000000000002220 ) ) ;
#76289=CARTESIAN_POINT ( 'NONE',  ( -113.6228709571500417, -23.48783264082479150, -1.443836473390060160 ) ) ;
#76290=CARTESIAN_POINT ( 'NONE',  ( -79.46053308078880661, -25.27791892412682984, 7.192626743707448256 ) ) ;
#76293=CARTESIAN_POINT ( 'NONE',  ( -16.26263985875334228, -10.51264992557365829, -1.500000000000002220 ) ) ;
#76294=CARTESIAN_POINT ( 'NONE',  ( -45.66178508354857968, -23.85016227208580375, -0.8807180028928391913 ) ) ;
#76295=VERTEX_POINT ( 'NONE', #10421 ) ;
#76296=CARTESIAN_POINT ( 'NONE',  ( -7.106217341473486826, 18.08270997100935418, 11.49999999999999645 ) ) ;
#76297=CARTESIAN_POINT ( 'NONE',  ( -108.2228709571500644, -23.47596703998600631, 11.44779298504227860 ) ) ;
#76301=FACE_OUTER_BOUND ( 'NONE', #31251, .T. ) ;
#76302=CARTESIAN_POINT ( 'NONE',  ( -130.5728709571500303, -23.47596703998600276, 11.44779298504227505 ) ) ;
#76303=CARTESIAN_POINT ( 'NONE',  ( -16.92291128558595048, 9.936001969431544012, 11.49999999999998934 ) ) ;
#76304=CARTESIAN_POINT ( 'NONE',  ( -66.52287095715006160, -23.48786465467241769, 11.44779295918254647 ) ) ;
#76305=ORIENTED_EDGE ( 'NONE', *, *, #38409, .T. ) ;
#76306=CARTESIAN_POINT ( 'NONE',  ( -8.857468890034409625, -19.66367526556523870, -1.500000000000002220 ) ) ;
#76308=CARTESIAN_POINT ( 'NONE',  ( -40.48996144562239863, -24.40034930558990922, 0.3402023900116037947 ) ) ;
#76311=CARTESIAN_POINT ( 'NONE',  ( -5.126879528927636542, -22.49243673399587351, -1.500000000000002220 ) ) ;
#76312=EDGE_CURVE ( 'NONE', #36801, #25844, #62970, .T. ) ;
#76314=CARTESIAN_POINT ( 'NONE',  ( -93.54681100557382933, -24.51314013834316796, 0.6176544820404163971 ) ) ;
#76315=CARTESIAN_POINT ( 'NONE',  ( -49.53589543791687788, -24.51314013834316086, 0.6176544820404130665 ) ) ;
#76316=CARTESIAN_POINT ( 'NONE',  ( -19.13055903301823335, -6.388282315271819556, 11.49999999999999645 ) ) ;
#76319=CARTESIAN_POINT ( 'NONE',  ( -111.7736932848194726, -25.29824102673524067, 4.173604034445157929 ) ) ;
#76320=CARTESIAN_POINT ( 'NONE',  ( -32.62287095715004881, -24.64898659630367206, 1.056161002820817485 ) ) ;
#76321=CARTESIAN_POINT ( 'NONE',  ( -76.62287095715007013, -23.48783264082478084, -1.443836473390065489 ) ) ;
#76322=CARTESIAN_POINT ( 'NONE',  ( 19.88832268942539017, -0.5522253751840191516, 11.49999999999998934 ) ) ;
#76324=EDGE_CURVE ( 'NONE', #84765, #84975, #99243, .T. ) ;
#76325=CARTESIAN_POINT ( 'NONE',  ( -5.448126336921106372, -18.99418723138115084, -1.500000000000002220 ) ) ;
#76326=EDGE_CURVE ( 'NONE', #69692, #67443, #48397, .T. ) ;
#76327=CARTESIAN_POINT ( 'NONE',  ( -42.53975314095062288, -24.34968618360933590, 0.1864209137778841952 ) ) ;
#76328=EDGE_CURVE ( 'NONE', #20641, #23622, #57120, .T. ) ;
#76331=EDGE_CURVE ( 'NONE', #43735, #11601, #99038, .T. ) ;
#76332=CARTESIAN_POINT ( 'NONE',  ( -40.07089665442598658, -25.10925601320060352, 2.873458142001279914 ) ) ;
#76334=CARTESIAN_POINT ( 'NONE',  ( 2.909938941155331360, -20.50406750007545398, 11.49999999999999645 ) ) ;
#76335=CARTESIAN_POINT ( 'NONE',  ( -58.52287095715004739, -23.47593901973090169, -1.443836447538997092 ) ) ;
#76337=CARTESIAN_POINT ( 'NONE',  ( 17.32531159343115945, 14.66459048539768162, 11.49999999999999645 ) ) ;
#76338=ORIENTED_EDGE ( 'NONE', *, *, #94435, .T. ) ;
#76339=CARTESIAN_POINT ( 'NONE',  ( -60.62287095715004881, -25.00158670708908915, 2.256160236439166855 ) ) ;
#76340=CARTESIAN_POINT ( 'NONE',  ( -70.19984806589197035, -25.12381722767544190, 7.096917652772970264 ) ) ;
#76341=CARTESIAN_POINT ( 'NONE',  ( -20.08517628505838815, -1.856936949192496300, -1.500000000000002220 ) ) ;
#76343=CARTESIAN_POINT ( 'NONE',  ( -63.58766835849188936, -24.34968618360933590, 0.1864209137778804204 ) ) ;
#76344=PLANE ( 'NONE',  #28567 ) ;
#76346=VERTEX_POINT ( 'NONE', #86046 ) ;
#76349=CARTESIAN_POINT ( 'NONE',  ( 22.81499323874321661, -2.031749852351878882, 11.49999999999998934 ) ) ;
#76350=CARTESIAN_POINT ( 'NONE',  ( -50.49777224651334961, -25.27420563618652238, 3.296419135251263732 ) ) ;
#76351=CARTESIAN_POINT ( 'NONE',  ( 5.568959250215116619, -20.88136358707659923, -1.500000000000002220 ) ) ;
#76352=FACE_OUTER_BOUND ( 'NONE', #9354, .T. ) ;
#76354=CARTESIAN_POINT ( 'NONE',  ( -19.40224465947428456, -7.824916089261592766, 11.49999999999999645 ) ) ;
#76356=CARTESIAN_POINT ( 'NONE',  ( -70.27422298781921484, -25.31612420447723011, 4.851635139248643647 ) ) ;
#76357=CARTESIAN_POINT ( 'NONE',  ( 7.855769811932122870, -20.56199346058834720, 11.49999999999998934 ) ) ;
#76358=ADVANCED_FACE ( 'NONE', ( #80439 ), #47494, .T. ) ;
#76360=CARTESIAN_POINT ( 'NONE',  ( -27.75582626765746497, -24.79700316727673126, 7.602201205707691756 ) ) ;
#76361=VERTEX_POINT ( 'NONE', #70831 ) ;
#76363=CARTESIAN_POINT ( 'NONE',  ( -90.58449365438282541, -24.83644354573578994, 8.397322867130100121 ) ) ;
#76364=ORIENTED_EDGE ( 'NONE', *, *, #98386, .T. ) ;
#76365=CARTESIAN_POINT ( 'NONE',  ( -72.63059420557763701, -24.35071581493543036, 9.817618358456032368 ) ) ;
#76366=EDGE_LOOP ( 'NONE', ( #21203, #79167, #44473, #44430 ) ) ;
#76368=CARTESIAN_POINT ( 'NONE',  ( -59.62287095715004881, -23.47593901973091235, -1.443836447539007972 ) ) ;
#76369=CARTESIAN_POINT ( 'NONE',  ( -95.62287095715004170, -24.63345952396256777, 9.038047939301502964 ) ) ;
#76370=CARTESIAN_POINT ( 'NONE',  ( -57.54252097118408216, -24.34968618360933590, 0.1864209137778796155 ) ) ;
#76371=CARTESIAN_POINT ( 'NONE',  ( 8.813945691637787405, 18.49579627399651471, -1.500000000000002220 ) ) ;
#76373=ORIENTED_EDGE ( 'NONE', *, *, #48536, .T. ) ;
#76375=B_SPLINE_CURVE_WITH_KNOTS ( 'NONE', 3,
 ( #14067, #6472, #68374, #29802 ),
 .UNSPECIFIED., .F., .F.,
 ( 4, 4 ),
 ( 0.000000000000000000, 0.0001000000000000167422 ),
 .UNSPECIFIED. ) ;
#76376=CARTESIAN_POINT ( 'NONE',  ( -60.62287095715004881, -23.47593901973091235, -1.443836447539007972 ) ) ;
#76378=CARTESIAN_POINT ( 'NONE',  ( 19.02167141253037030, -11.55642654327076535, 11.49999999999998934 ) ) ;
#76381=CARTESIAN_POINT ( 'NONE',  ( -88.62287095715004170, -23.96177878511308634, 10.65340807706329507 ) ) ;
#76382=ORIENTED_EDGE ( 'NONE', *, *, #38645, .F. ) ;
#76384=CARTESIAN_POINT ( 'NONE',  ( -28.66728577581702808, -24.63646007072033228, 7.986660916366364660 ) ) ;
#76385=CARTESIAN_POINT ( 'NONE',  ( 20.75994597877129877, -1.272245555857973054, -1.500000000000002220 ) ) ;
#76386=AXIS2_PLACEMENT_3D ( 'NONE', #98666, #91061, #52512 ) ;
#76387=ORIENTED_EDGE ( 'NONE', *, *, #34067, .F. ) ;
#76392=ORIENTED_EDGE ( 'NONE', *, *, #93816, .T. ) ;
#76395=CARTESIAN_POINT ( 'NONE',  ( -118.1692044365139367, -25.21250203164488468, 3.500954016957965820 ) ) ;
#76396=CARTESIAN_POINT ( 'NONE',  ( -100.7317701684513764, -25.25419550244751221, 7.544845661441120122 ) ) ;
#76397=CARTESIAN_POINT ( 'NONE',  ( -91.62287095715004170, -23.47593901973091235, -1.443836447539002865 ) ) ;
#76398=FACE_OUTER_BOUND ( 'NONE', #67820, .T. ) ;
#76399=CARTESIAN_POINT ( 'NONE',  ( 21.58644828898399481, -4.983269013152989757, 11.49999999999999645 ) ) ;
#76400=ORIENTED_EDGE ( 'NONE', *, *, #4819, .T. ) ;
#76402=CARTESIAN_POINT ( 'NONE',  ( -11.22117850230010738, 19.66027149220947123, -1.500000000000002220 ) ) ;
#76403=CARTESIAN_POINT ( 'NONE',  ( -36.62287095715005592, -24.64898659630367916, 1.056161002820819261 ) ) ;
#76410=B_SPLINE_CURVE_WITH_KNOTS ( 'NONE', 3,
 ( #76273, #51464, #82399, #66212 ),
 .UNSPECIFIED., .F., .F.,
 ( 4, 4 ),
 ( 0.000000000000000000, 0.0001000000000000444977 ),
 .UNSPECIFIED. ) ;
#76411=CARTESIAN_POINT ( 'NONE',  ( -18.22032804147677254, 8.545885342870345625, 11.49999999999998934 ) ) ;
#76412=LINE ( 'NONE', #8414, #11693 ) ;
#76413=ORIENTED_EDGE ( 'NONE', *, *, #93165, .T. ) ;
#76415=CARTESIAN_POINT ( 'NONE',  ( -18.97848940637192428, 11.77069306843248064, -1.500000000000002220 ) ) ;
#76418=FACE_OUTER_BOUND ( 'NONE', #46959, .T. ) ;
#76419=CARTESIAN_POINT ( 'NONE',  ( -119.5895376238167387, -23.48786465467241769, 11.44779295918253759 ) ) ;
#76420=CARTESIAN_POINT ( 'NONE',  ( -85.58953762381672448, -23.47596703998600631, 11.44779298504227683 ) ) ;
#76423=CARTESIAN_POINT ( 'NONE',  ( 12.76379665850700640, 14.79237594083867080, -1.500000000000002220 ) ) ;
#76425=CARTESIAN_POINT ( 'NONE',  ( -11.48222599368078889, -18.13851731312990267, 11.49999999999998934 ) ) ;
#76427=CARTESIAN_POINT ( 'NONE',  ( -46.52287095715006160, -23.47596703998600631, 11.44779298504229104 ) ) ;
#76428=CARTESIAN_POINT ( 'NONE',  ( -118.5228709571500758, -23.47593901973090524, -1.443836447538996204 ) ) ;
#76429=B_SPLINE_CURVE_WITH_KNOTS ( 'NONE', 3,
 ( #10404, #10913, #72316, #64219, #64731, #94639, #95145, #42384, #24616, #17011, #25632, #49489, #40853, #95647 ),
 .UNSPECIFIED., .F., .F.,
 ( 4, 2, 2, 2, 2, 2, 4 ),
 ( 1.411962612463446054E-17, 0.0001805495034875036512, 0.0003610990069749931536, 0.0007221980139500113523, 0.001083297020925029714, 0.001263846524412529570, 0.001444396027900029860 ),
 .UNSPECIFIED. ) ;
#76430=CARTESIAN_POINT ( 'NONE',  ( 7.980177114813061579, 21.45908683785374649, -1.500000000000002220 ) ) ;
#76433=CARTESIAN_POINT ( 'NONE',  ( -120.5895376238167245, -25.00158670708909980, 2.256160236439166411 ) ) ;
#76435=CARTESIAN_POINT ( 'NONE',  ( -12.66726347749767179, -15.43046242340049545, 11.49999999999999645 ) ) ;
#76436=CARTESIAN_POINT ( 'NONE',  ( -120.5228709571500616, -29.50248528299804818, 1.056150453629045360 ) ) ;
#76437=EDGE_CURVE ( 'NONE', #50685, #45688, #58604, .T. ) ;
#76438=EDGE_CURVE ( 'NONE', #96494, #87248, #66238, .T. ) ;
#76439=CARTESIAN_POINT ( 'NONE',  ( -63.52287095715003318, -23.48783264082477018, -1.443836473390091690 ) ) ;
#76440=PLANE ( 'NONE',  #35915 ) ;
#76441=EDGE_LOOP ( 'NONE', ( #4884, #11477, #97385, #81238 ) ) ;
#76443=CARTESIAN_POINT ( 'NONE',  ( -65.52287095715009002, -24.92604778743017491, 8.074972756849353672 ) ) ;
#76445=CARTESIAN_POINT ( 'NONE',  ( -20.56741719582323213, 7.008553436993695485, -1.500000000000002220 ) ) ;
#76446=CARTESIAN_POINT ( 'NONE',  ( -78.52287095715006160, -23.48786465467241769, 11.44779295918254469 ) ) ;
#76447=CARTESIAN_POINT ( 'NONE',  ( -11.77723790057865116, -15.68276428244051779, -1.500000000000002220 ) ) ;
#76449=CARTESIAN_POINT ( 'NONE',  ( -99.89883556272337728, -25.14992886684538931, 7.003669732127485226 ) ) ;
#76450=ADVANCED_FACE ( 'NONE', ( #67727 ), #7800, .F. ) ;
#76452=LINE ( 'NONE', #6957, #4653 ) ;
#76454=CARTESIAN_POINT ( 'NONE',  ( -7.444040098415714013, -19.11467064512029879, 11.49999999999999645 ) ) ;
#76457=FACE_OUTER_BOUND ( 'NONE', #1132, .T. ) ;
#76459=CARTESIAN_POINT ( 'NONE',  ( -30.48631411044201656, -23.47596703823905528, 11.44698924286007369 ) ) ;
#76462=FACE_OUTER_BOUND ( 'NONE', #11714, .T. ) ;
#76466=B_SPLINE_CURVE_WITH_KNOTS ( 'NONE', 3,
 ( #23894, #79686, #86799, #10183, #25404, #79184 ),
 .UNSPECIFIED., .F., .F.,
 ( 4, 2, 4 ),
 ( 6.391158118959990520E-06, 0.001387004593080781592, 0.002767618028042603297 ),
 .UNSPECIFIED. ) ;
#76468=EDGE_CURVE ( 'NONE', #76683, #98076, #20318, .T. ) ;
#76469=CARTESIAN_POINT ( 'NONE',  ( 10.36671515591691950, -20.60271000134967068, 11.49999999999999645 ) ) ;
#76470=CARTESIAN_POINT ( 'NONE',  ( 18.64237364862239943, 13.12531859369229359, -1.500000000000002220 ) ) ;
#76472=CARTESIAN_POINT ( 'NONE',  ( -105.6228709571500843, -24.51163499207180507, 0.6490370598555564863 ) ) ;
#76473=CARTESIAN_POINT ( 'NONE',  ( -104.5562042904833930, -24.66019654487199730, 8.947790411086124607 ) ) ;
#76475=CARTESIAN_POINT ( 'NONE',  ( -110.2929128916653525, -25.15277794460069316, 6.986250878905948980 ) ) ;
#76476=CARTESIAN_POINT ( 'NONE',  ( -99.50663065733192525, -25.31582213395984837, 4.996268174089572689 ) ) ;
#76477=CARTESIAN_POINT ( 'NONE',  ( -3.478157889954244464, -21.63767827151469447, 11.49999999999998934 ) ) ;
#76479=CARTESIAN_POINT ( 'NONE',  ( -87.51421109775209572, -23.96169478059713498, 10.65365249895718058 ) ) ;
#76481=CARTESIAN_POINT ( 'NONE',  ( -78.55878933397490016, -23.73766607897670511, -1.055555164236459342 ) ) ;
#76482=CARTESIAN_POINT ( 'NONE',  ( -117.6228709571500559, -23.72747288104441665, -1.053458166803660667 ) ) ;
#76484=CARTESIAN_POINT ( 'NONE',  ( 20.35601985306173134, -1.938729116259007679, 11.49999999999998934 ) ) ;
#76485=EDGE_LOOP ( 'NONE', ( #15071, #4183, #40238, #42458 ) ) ;
#76486=ORIENTED_EDGE ( 'NONE', *, *, #14227, .T. ) ;
#76487=ORIENTED_EDGE ( 'NONE', *, *, #91288, .F. ) ;
#76488=ORIENTED_EDGE ( 'NONE', *, *, #20837, .T. ) ;
#76489=CARTESIAN_POINT ( 'NONE',  ( -21.01138170180016118, -9.542296329091309204, 11.49999999999998934 ) ) ;
#76490=CARTESIAN_POINT ( 'NONE',  ( -41.48151182693364802, -25.18341647909762671, 3.283321612209681550 ) ) ;
#76491=CARTESIAN_POINT ( 'NONE',  ( 12.36038202409810438, -16.04522380935875248, -1.500000000000002220 ) ) ;
#76493=CARTESIAN_POINT ( 'NONE',  ( -29.26901259668666100, -25.11027012358568911, 6.759032221908313431 ) ) ;
#76494=CARTESIAN_POINT ( 'NONE',  ( -46.62287095715004881, -24.64898659630528499, 1.056161002820821038 ) ) ;
#76495=ADVANCED_FACE ( 'NONE', ( #13907 ), #44885, .T. ) ;
#76496=CARTESIAN_POINT ( 'NONE',  ( -93.62287095715007013, -23.47596703998600631, 11.44779298504227860 ) ) ;
#76497=CARTESIAN_POINT ( 'NONE',  ( -70.54637579065081354, -24.40034930558990922, 0.3402023900116040167 ) ) ;
#76498=CARTESIAN_POINT ( 'NONE',  ( 0.5228555243449846124, 21.43159495547403282, 11.49999999999999645 ) ) ;
#76499=VERTEX_POINT ( 'NONE', #6307 ) ;
#76500=CARTESIAN_POINT ( 'NONE',  ( -48.52287095715006160, -29.50248528299804818, 1.056150453629033370 ) ) ;
#76501=CARTESIAN_POINT ( 'NONE',  ( -61.60404647597454186, -23.73791477778911840, 11.05961554403170943 ) ) ;
#76502=ORIENTED_EDGE ( 'NONE', *, *, #24224, .T. ) ;
#76503=CARTESIAN_POINT ( 'NONE',  ( -18.06733440434376092, 10.15830956056102963, -1.500000000000002220 ) ) ;
#76505=VERTEX_POINT ( 'NONE', #22507 ) ;
#76507=ORIENTED_EDGE ( 'NONE', *, *, #82199, .F. ) ;
#76509=B_SPLINE_SURFACE_WITH_KNOTS ( 'NONE', 3, 3, ( 
 ( #51017, #58138, #33275, #42908 ),
 ( #95184, #88080, #11444, #4344 ),
 ( #73354, #34788, #35294, #41402 ),
 ( #57143, #72857, #49526, #27677 ),
 ( #81953, #12437, #90561, #22028 ),
 ( #5325, #36288, #21041, #66758 ),
 ( #60634, #97676, #13429, #68730 ) ),
 .UNSPECIFIED., .F., .F., .F.,
 ( 4, 3, 4 ),
 ( 4, 4 ),
 ( 0.7945040050992250302, 0.8970133687736510097, 0.9995227324480769893 ),
 ( 0.9797429635068189979, 0.9812080024286750080 ),
 .UNSPECIFIED. ) ;
#76511=EDGE_LOOP ( 'NONE', ( #91744, #35945, #17398, #25386 ) ) ;
#76512=CARTESIAN_POINT ( 'NONE',  ( -55.52287095715006160, -24.91570333825770689, 8.075032458260354318 ) ) ;
#76513=CARTESIAN_POINT ( 'NONE',  ( -65.50513712851758896, -24.15503026093916361, -0.2815557561904382111 ) ) ;
#76514=CARTESIAN_POINT ( 'NONE',  ( 0.3405503412851532130, 21.98688381012616233, 11.49999999999999645 ) ) ;
#76516=CARTESIAN_POINT ( 'NONE',  ( 21.16815136333514502, -7.790938087775149512, 11.49999999999998934 ) ) ;
#76517=CARTESIAN_POINT ( 'NONE',  ( -4.092705237139750984, -20.55955383578756113, 11.49999999999998934 ) ) ;
#76518=CARTESIAN_POINT ( 'NONE',  ( -109.1607220907064004, -25.31604877966584155, 4.925676078390490709 ) ) ;
#76520=ORIENTED_EDGE ( 'NONE', *, *, #17155, .T. ) ;
#76522=ORIENTED_EDGE ( 'NONE', *, *, #59809, .F. ) ;
#76523=EDGE_LOOP ( 'NONE', ( #61832, #38440, #31220, #94706 ) ) ;
#76525=DIRECTION ( 'NONE',  ( -0.8369330630277744820, 1.189580657286399882E-06, -0.5473052603525132564 ) ) ;
#76526=CARTESIAN_POINT ( 'NONE',  ( 16.66814584454133907, -13.58961022886752978, -1.500000000000002220 ) ) ;
#76527=CARTESIAN_POINT ( 'NONE',  ( -90.62287095715004170, -23.84081130438200091, 10.88220057463249191 ) ) ;
#76528=VERTEX_POINT ( 'NONE', #14902 ) ;
#76529=CARTESIAN_POINT ( 'NONE',  ( 13.68530018921192060, -16.06810839794082924, -1.500000000000002220 ) ) ;
#76530=CARTESIAN_POINT ( 'NONE',  ( -127.6228709571500559, -29.50250243563736774, 8.947779886222132717 ) ) ;
#76531=CARTESIAN_POINT ( 'NONE',  ( -64.60341764832335798, -23.73766607897670156, -1.055555164236459564 ) ) ;
#76532=CARTESIAN_POINT ( 'NONE',  ( -83.60405270194971195, -23.48786465467241413, 11.44779295918254469 ) ) ;
#76534=CARTESIAN_POINT ( 'NONE',  ( -99.66129388137581202, -25.14737294716416471, 3.044676272356992008 ) ) ;
#76535=CARTESIAN_POINT ( 'NONE',  ( -7.477829544921322125, 20.88912457518834742, -1.500000000000002220 ) ) ;
#76537=ORIENTED_EDGE ( 'NONE', *, *, #94440, .T. ) ;
#76538=CARTESIAN_POINT ( 'NONE',  ( -51.77186309286971522, -25.31633219839644156, 5.562993592441398683 ) ) ;
#76539=CARTESIAN_POINT ( 'NONE',  ( -73.52287095715007581, -24.66019654487199730, 8.947790411086121054 ) ) ;
#76540=CARTESIAN_POINT ( 'NONE',  ( -43.62287095715004881, -24.65952944569304606, 1.056160979905692576 ) ) ;
#76541=DIRECTION ( 'NONE',  ( 0.000000000000000000, -0.9999999999976377785, -2.173523156925979975E-06 ) ) ;
#76542=VECTOR ( 'NONE', #14529, 1000.000000000000114 ) ;
#76543=CARTESIAN_POINT ( 'NONE',  ( 5.650214204171827070, -18.61605495904187535, 11.49999999999998934 ) ) ;
#76545=CARTESIAN_POINT ( 'NONE',  ( -20.51402961445061734, 6.013860829077147585, -1.500000000000002220 ) ) ;
#76546=CARTESIAN_POINT ( 'NONE',  ( -62.49924954558335344, -24.34968618360933945, 0.1864209137778798930 ) ) ;
#76550=CARTESIAN_POINT ( 'NONE',  ( 4.564784964189898098, -22.25151590922551748, -1.500000000000002220 ) ) ;
#76551=AXIS2_PLACEMENT_3D ( 'NONE', #67352, #97783, #28275 ) ;
#76552=EDGE_LOOP ( 'NONE', ( #34222, #88659, #35594, #17358 ) ) ;
#76554=DIRECTION ( 'NONE',  ( 0.000000000000000000, -2.173523156925980399E-06, 0.9999999999976378895 ) ) ;
#76555=CARTESIAN_POINT ( 'NONE',  ( -17.21045110277357182, -9.822940424218707278, 11.49999999999999645 ) ) ;
#76558=LINE ( 'NONE', #6568, #3617 ) ;
#76559=B_SPLINE_CURVE_WITH_KNOTS ( 'NONE', 3,
 ( #65915, #80609, #50666, #11099, #96832, #73502 ),
 .UNSPECIFIED., .F., .F.,
 ( 4, 2, 4 ),
 ( 6.384118678604741492E-06, 0.001386860460828369997, 0.002767336802978134520 ),
 .UNSPECIFIED. ) ;
#76564=CARTESIAN_POINT ( 'NONE',  ( 19.28387207504633949, -9.851753786812027514, 11.49999999999998934 ) ) ;
#76565=DIRECTION ( 'NONE',  ( 3.773278334444166432E-23, -1.000000000000000000, 0.000000000000000000 ) ) ;
#76566=CARTESIAN_POINT ( 'NONE',  ( 16.42231304340664266, 10.40281881132301045, -1.500000000000002220 ) ) ;
#76567=B_SPLINE_CURVE_WITH_KNOTS ( 'NONE', 3,
 ( #95001, #93997, #3178, #55453 ),
 .UNSPECIFIED., .F., .F.,
 ( 4, 4 ),
 ( 0.2907075871721704341, 0.2997140184442859678 ),
 .UNSPECIFIED. ) ;
#76568=EDGE_CURVE ( 'NONE', #93974, #48086, #64047, .T. ) ;
#76570=CARTESIAN_POINT ( 'NONE',  ( -82.62287095715007013, -24.66019654487199375, 8.947790411086128159 ) ) ;
#76571=CARTESIAN_POINT ( 'NONE',  ( 6.388261542594571019, -18.74682169789839392, -1.500000000000002220 ) ) ;
#76572=EDGE_LOOP ( 'NONE', ( #51338, #81894, #41388, #47961 ) ) ;
#76574=CARTESIAN_POINT ( 'NONE',  ( -13.46841296510753061, 15.22696965993213070, 11.49999999999999645 ) ) ;
#76575=FACE_OUTER_BOUND ( 'NONE', #35987, .T. ) ;
#76576=EDGE_CURVE ( 'NONE', #14843, #44696, #61506, .T. ) ;
#76578=EDGE_LOOP ( 'NONE', ( #34849, #52804, #28415, #69499 ) ) ;
#76579=CARTESIAN_POINT ( 'NONE',  ( -0.1187647035275026935, -21.51249758272363621, -1.017619990082605952 ) ) ;
#76580=DIRECTION ( 'NONE',  ( 0.000000000000000000, -0.9999999999976377785, -2.173523156925979975E-06 ) ) ;
#76581=CARTESIAN_POINT ( 'NONE',  ( -48.95379770480546711, -25.25214592170422279, 5.698183657943237890 ) ) ;
#76583=CARTESIAN_POINT ( 'NONE',  ( -82.52287095715006160, -23.47596703998600631, 11.44779298504228571 ) ) ;
#76584=CARTESIAN_POINT ( 'NONE',  ( -18.39468835979788608, -8.022455445098881199, 11.49999999999998934 ) ) ;
#76585=EDGE_CURVE ( 'NONE', #43203, #27745, #96732, .T. ) ;
#76590=CARTESIAN_POINT ( 'NONE',  ( 0.5590224530292132732, -22.91010021869659852, 11.49999999999999645 ) ) ;
#76591=CARTESIAN_POINT ( 'NONE',  ( 18.72737137862276313, -12.84423604280260278, -1.500000000000002220 ) ) ;
#76592=CARTESIAN_POINT ( 'NONE',  ( -30.47287095715008221, -24.04764615585419207, -0.4449263091658831604 ) ) ;
#76593=AXIS2_PLACEMENT_3D ( 'NONE', #86325, #31530, #85824 ) ;
#76595=CARTESIAN_POINT ( 'NONE',  ( -38.58103285119013037, -24.51419770103157703, 9.386484678747176957 ) ) ;
#76598=DIRECTION ( 'NONE',  ( -1.000000000000000000, -3.773278334444167608E-23, -8.201307833595939069E-29 ) ) ;
#76600=CARTESIAN_POINT ( 'NONE',  ( 19.83649001621966335, 4.521578618930774951, 11.49999999999998934 ) ) ;
#76601=ORIENTED_EDGE ( 'NONE', *, *, #47500, .F. ) ;
#76603=CARTESIAN_POINT ( 'NONE',  ( 20.74614131242519477, 9.816050768296040729, -1.500000000000002220 ) ) ;
#76604=CARTESIAN_POINT ( 'NONE',  ( -78.62287095715005592, -29.50247984919015209, -1.443849546365053582 ) ) ;
#76607=CARTESIAN_POINT ( 'NONE',  ( -77.55021002596484436, -24.15620529776628800, 10.23563542870659937 ) ) ;
#76608=CARTESIAN_POINT ( 'NONE',  ( -51.50148419838348701, -24.15620529776627734, 10.23563542870660470 ) ) ;
#76609=CARTESIAN_POINT ( 'NONE',  ( 1.567330217057175901, -21.20382687294985047, 11.49999999999999645 ) ) ;
#76610=ORIENTED_EDGE ( 'NONE', *, *, #97862, .F. ) ;
#76612=VERTEX_POINT ( 'NONE', #40755 ) ;
#76613=CARTESIAN_POINT ( 'NONE',  ( 4.129723114849880083, -21.82631191821171512, -1.500000000000002220 ) ) ;
#76614=CARTESIAN_POINT ( 'NONE',  ( -20.24099117049231467, 3.958469829285517161, -1.500000000000002220 ) ) ;
#76617=VERTEX_POINT ( 'NONE', #32134 ) ;
#76619=EDGE_CURVE ( 'NONE', #5489, #89924, #59179, .T. ) ;
#76620=CARTESIAN_POINT ( 'NONE',  ( -36.62287095715005592, -24.64898659630367916, 1.056161002820819261 ) ) ;
#76622=CARTESIAN_POINT ( 'NONE',  ( -49.68342748179477297, -25.16659734855911523, 6.901253476643402607 ) ) ;
#76625=CARTESIAN_POINT ( 'NONE',  ( -126.7287200997190837, -25.23482084814632387, 3.690491797312001943 ) ) ;
#76626=CARTESIAN_POINT ( 'NONE',  ( -88.62287095715002749, -24.66019654487199730, 8.947790411086128159 ) ) ;
#76627=CARTESIAN_POINT ( 'NONE',  ( -14.03827505669662479, 15.38897104800697591, -1.500000000000002220 ) ) ;
#76628=CARTESIAN_POINT ( 'NONE',  ( 6.829227106855087825, -20.66181959361685827, 11.49999999999999645 ) ) ;
#76630=CARTESIAN_POINT ( 'NONE',  ( -40.39532865008378337, -25.18518669035473323, 3.295758758853348791 ) ) ;
#76631=CARTESIAN_POINT ( 'NONE',  ( -71.52287095715007581, -24.65952944569304606, 1.056160979905697239 ) ) ;
#76632=CARTESIAN_POINT ( 'NONE',  ( -18.83616483605274539, -12.25834331966736102, -1.500000000000002220 ) ) ;
#76633=CARTESIAN_POINT ( 'NONE',  ( -51.26061221361337061, -25.26334635016775465, 4.199398795162026410 ) ) ;
#76634=ORIENTED_EDGE ( 'NONE', *, *, #58977, .F. ) ;
#76637=B_SPLINE_SURFACE_WITH_KNOTS ( 'NONE', 3, 3, ( 
 ( #29556, #12333, #36677, #29058 ),
 ( #67641, #74243, #14321, #98563 ),
 ( #66663, #4240, #52406, #83342 ),
 ( #13825, #6219, #46285, #94838 ),
 ( #100043, #76710, #40568, #38161 ),
 ( #68629, #30554, #79111, #33440 ),
 ( #61024, #64428, #10106, #48181 ) ),
 .UNSPECIFIED., .F., .F., .F.,
 ( 4, 3, 4 ),
 ( 4, 4 ),
 ( 0.0004766839783822563858, 0.1029713700210899974, 0.2054660560637977251 ),
 ( 0.07951422430824672816, 0.08056363658127665972 ),
 .UNSPECIFIED. ) ;
#76641=ORIENTED_EDGE ( 'NONE', *, *, #41518, .T. ) ;
#76642=CARTESIAN_POINT ( 'NONE',  ( -20.89022842043660688, 4.291957016416017900, -1.500000000000002220 ) ) ;
#76644=CARTESIAN_POINT ( 'NONE',  ( -19.58807393344005376, -7.628504261335002923, 11.49999999999998934 ) ) ;
#76645=CARTESIAN_POINT ( 'NONE',  ( -30.41986401503926274, -24.82632770740921302, 1.633466014234818076 ) ) ;
#76646=CARTESIAN_POINT ( 'NONE',  ( -41.46355252140796210, -25.18431046067977874, 4.097885018056865114 ) ) ;
#76647=CARTESIAN_POINT ( 'NONE',  ( -65.52287095715006160, -23.47596703998600631, 11.44779298504228748 ) ) ;
#76648=CARTESIAN_POINT ( 'NONE',  ( 3.689792033372774060, 21.67897595795444587, -1.500000000000002220 ) ) ;
#76649=CARTESIAN_POINT ( 'NONE',  ( -87.59490587792481620, -23.96119346886882084, -0.6495511937831871530 ) ) ;
#76650=ORIENTED_EDGE ( 'NONE', *, *, #21007, .F. ) ;
#76651=FACE_OUTER_BOUND ( 'NONE', #67583, .T. ) ;
#76652=VECTOR ( 'NONE', #38593, 1000.000000000000114 ) ;
#76654=CARTESIAN_POINT ( 'NONE',  ( -84.56294652207583340, -23.48786465467241769, 11.44779295918254647 ) ) ;
#76655=CARTESIAN_POINT ( 'NONE',  ( -130.5728709571501724, -25.14064729901805251, 2.712351064733618866 ) ) ;
#76656=CARTESIAN_POINT ( 'NONE',  ( -20.43222813077822408, -23.69307752509138965, 9.440663514584134219 ) ) ;
#76657=CARTESIAN_POINT ( 'NONE',  ( -9.338289970059909351, 19.12570833482435617, -1.500000000000002220 ) ) ;
#76658=PLANE ( 'NONE',  #20733 ) ;
#76659=DIRECTION ( 'NONE',  ( -3.773278334453080206E-23, 0.9999999999976377785, 2.173523156925979975E-06 ) ) ;
#76660=CARTESIAN_POINT ( 'NONE',  ( -90.62287095715004170, -23.47593901973091235, -1.443836447539002865 ) ) ;
#76661=CARTESIAN_POINT ( 'NONE',  ( -33.52641739661655151, -24.65952944569304606, 1.056160979905695907 ) ) ;
#76662=CARTESIAN_POINT ( 'NONE',  ( 1.861690257272737847, 22.46465895387273903, -1.500000000000002220 ) ) ;
#76664=VERTEX_POINT ( 'NONE', #88935 ) ;
#76666=CARTESIAN_POINT ( 'NONE',  ( 13.00645856128228495, 14.71372164842801844, 11.49999999999999645 ) ) ;
#76669=ORIENTED_EDGE ( 'NONE', *, *, #4204, .F. ) ;
#76670=CARTESIAN_POINT ( 'NONE',  ( -88.58575907974172026, -24.51419770103157703, 9.386484678747176957 ) ) ;
#76671=CARTESIAN_POINT ( 'NONE',  ( -126.7289109336821866, -25.33574223958540017, 6.311323082738798718 ) ) ;
#76672=CARTESIAN_POINT ( 'NONE',  ( -88.87103898935609436, -25.22174524493127734, 6.695141717414601068 ) ) ;
#76674=CARTESIAN_POINT ( 'NONE',  ( -9.502044936771568473, -17.27029980899984452, 11.49999999999998934 ) ) ;
#76675=B_SPLINE_CURVE_WITH_KNOTS ( 'NONE', 3,
 ( #17026, #9410, #40373, #100238 ),
 .UNSPECIFIED., .F., .F.,
 ( 4, 4 ),
 ( 0.000000000000000000, 9.999999999998897304E-05 ),
 .UNSPECIFIED. ) ;
#76676=ORIENTED_EDGE ( 'NONE', *, *, #8757, .F. ) ;
#76677=EDGE_CURVE ( 'NONE', #15184, #96261, #65621, .T. ) ;
#76679=FACE_OUTER_BOUND ( 'NONE', #88147, .T. ) ;
#76680=EDGE_CURVE ( 'NONE', #17192, #53455, #31302, .T. ) ;
#76683=VERTEX_POINT ( 'NONE', #19410 ) ;
#76684=CARTESIAN_POINT ( 'NONE',  ( -79.62287095715005592, -29.50247984919015209, -1.443849546365053582 ) ) ;
#76686=CARTESIAN_POINT ( 'NONE',  ( -55.48003037949258953, -24.92564183028978775, 1.928384488918253092 ) ) ;
#76691=B_SPLINE_CURVE_WITH_KNOTS ( 'NONE', 3,
 ( #86443, #85946, #84441, #99648 ),
 .UNSPECIFIED., .F., .F.,
 ( 4, 4 ),
 ( 0.000000000000000000, 9.999999999996123101E-05 ),
 .UNSPECIFIED. ) ;
#76692=DIRECTION ( 'NONE',  ( -3.773278334444167608E-23, 1.000000000000000000, 0.000000000000000000 ) ) ;
#76693=CARTESIAN_POINT ( 'NONE',  ( 19.98059151383774434, -0.7942727526097331792, 11.49999999999998934 ) ) ;
#76696=CARTESIAN_POINT ( 'NONE',  ( -51.68123905711060928, -25.28846605061042396, 4.189028613740050311 ) ) ;
#76698=CARTESIAN_POINT ( 'NONE',  ( -119.5893898853676802, -24.34968618360934656, 0.1864209137778924386 ) ) ;
#76701=CARTESIAN_POINT ( 'NONE',  ( -100.5228709571501184, -24.92604778743017846, 8.074972756849364330 ) ) ;
#76704=B_SPLINE_CURVE_WITH_KNOTS ( 'NONE', 3,
 ( #45698, #84245, #16242, #23336, #47203, #46704 ),
 .UNSPECIFIED., .F., .F.,
 ( 4, 2, 4 ),
 ( 1.570887131794638196E-05, 0.001396322306279758904, 0.002776935741241571502 ),
 .UNSPECIFIED. ) ;
#76705=B_SPLINE_SURFACE_WITH_KNOTS ( 'NONE', 3, 3, ( 
 ( #59573, #90504, #37221, #15365 ),
 ( #29597, #45341, #38207, #13870 ),
 ( #75273, #51954, #46328, #20982 ),
 ( #6757, #5766, #98608, #44841 ),
 ( #37713, #68671, #99592, #30095 ),
 ( #61068, #22466, #53457, #84385 ),
 ( #14865, #45833, #23464, #41226 ) ),
 .UNSPECIFIED., .F., .F., .F.,
 ( 4, 3, 4 ),
 ( 4, 4 ),
 ( 0.7945040050992236980, 0.8970133687736500105, 0.9995227324480763231 ),
 ( 0.6296540010513237418, 0.6309574156764954367 ),
 .UNSPECIFIED. ) ;
#76708=ORIENTED_EDGE ( 'NONE', *, *, #56606, .T. ) ;
#76709=CARTESIAN_POINT ( 'NONE',  ( -12.33117494125061242, 16.09929768045241261, 11.49999999999998934 ) ) ;
#76710=CARTESIAN_POINT ( 'NONE',  ( -122.5894821100217769, -24.34968618360934300, 0.1864209137778896352 ) ) ;
#76711=DIRECTION ( 'NONE',  ( -1.000000000000000000, -3.773278334444166432E-23, -8.201307841325785021E-29 ) ) ;
#76712=CARTESIAN_POINT ( 'NONE',  ( -105.6228709571500559, -24.92579138211018375, 1.929029949965666457 ) ) ;
#76714=PLANE ( 'NONE',  #50205 ) ;
#76716=CARTESIAN_POINT ( 'NONE',  ( -16.19606052442943067, -11.93128464602566474, -1.500000000000002220 ) ) ;
#76718=CARTESIAN_POINT ( 'NONE',  ( -8.250207518706217158, 19.40231308534122689, 11.49999999999999645 ) ) ;
#76719=CARTESIAN_POINT ( 'NONE',  ( -64.62287095715005592, -24.66019654487198665, 8.947790411086131712 ) ) ;
#76720=CARTESIAN_POINT ( 'NONE',  ( 18.18892703665305177, -12.56521834855340281, -1.500000000000002220 ) ) ;
#76721=EDGE_CURVE ( 'NONE', #29240, #34994, #18017, .T. ) ;
#76722=CARTESIAN_POINT ( 'NONE',  ( 20.52540449432101610, 0.9483640940595650104, -1.500000000000002220 ) ) ;
#76723=CARTESIAN_POINT ( 'NONE',  ( -61.24303164512834030, -25.04307381209219230, 7.563174986197129357 ) ) ;
#76725=EDGE_LOOP ( 'NONE', ( #3895, #28102, #34675, #57702 ) ) ;
#76727=ORIENTED_EDGE ( 'NONE', *, *, #19298, .F. ) ;
#76728=CARTESIAN_POINT ( 'NONE',  ( -96.62287095715005592, -29.50247984919015209, -1.443849546365050029 ) ) ;
#76729=CARTESIAN_POINT ( 'NONE',  ( -67.62287095715008434, -23.47596703998600276, 11.44779298504227505 ) ) ;
#76730=ORIENTED_EDGE ( 'NONE', *, *, #59876, .T. ) ;
#76732=VERTEX_POINT ( 'NONE', #50379 ) ;
#76733=CARTESIAN_POINT ( 'NONE',  ( -51.70072539166533687, -25.26311289191998455, 3.987152081390995306 ) ) ;
#76734=DIRECTION ( 'NONE',  ( 1.000000000000000000, 3.773278334444167608E-23, 8.201307833595939069E-29 ) ) ;
#76735=DIRECTION ( 'NONE',  ( -3.773278334453079618E-23, 0.9999999999976377785, 2.173523156925979552E-06 ) ) ;
#76736=CARTESIAN_POINT ( 'NONE',  ( 10.61356161029474521, 17.70173163822984819, -1.500000000000002220 ) ) ;
#76737=CARTESIAN_POINT ( 'NONE',  ( 4.348677445931066643, 21.19853102677161871, 11.49999999999999645 ) ) ;
#76738=ORIENTED_EDGE ( 'NONE', *, *, #81393, .F. ) ;
#76739=CARTESIAN_POINT ( 'NONE',  ( -80.35919894935767616, -25.29542306156489673, 4.505481338088394239 ) ) ;
#76741=CARTESIAN_POINT ( 'NONE',  ( -18.94483701893047467, 11.91932228829616669, 11.49999999999998934 ) ) ;
#76742=B_SPLINE_CURVE_WITH_KNOTS ( 'NONE', 3,
 ( #83314, #51383, #4710, #35663, #82324, #43774, #59495, #29526 ),
 .UNSPECIFIED., .F., .F.,
 ( 4, 2, 2, 4 ),
 ( -0.001224554619866350400, -0.0002241820295893703040, 0.0007761905606876097919, 0.002776935741241571068 ),
 .UNSPECIFIED. ) ;
#76743=CARTESIAN_POINT ( 'NONE',  ( -80.37464638460068045, -25.12205811127329014, 7.098502408654610463 ) ) ;
#76744=CARTESIAN_POINT ( 'NONE',  ( -84.54750306560438844, -24.34968618360934300, 0.1864209137778835013 ) ) ;
#76746=CARTESIAN_POINT ( 'NONE',  ( -60.62287095715004881, -24.99156045073392463, 7.747789690856161648 ) ) ;
#76747=CARTESIAN_POINT ( 'NONE',  ( -49.54715521573665171, -24.15620529776627379, 10.23563542870661003 ) ) ;
#76748=CARTESIAN_POINT ( 'NONE',  ( -115.5228709571500474, -24.91544648472620338, 1.928969306349230584 ) ) ;
#76749=CARTESIAN_POINT ( 'NONE',  ( -20.86263692406621928, 1.606387762444034362, 11.49999999999998934 ) ) ;
#76751=ADVANCED_FACE ( 'NONE', ( #58003 ), #28518, .F. ) ;
#76752=CARTESIAN_POINT ( 'NONE',  ( -86.59885310783221257, -23.73766607897671221, -1.055555164236432697 ) ) ;
#76755=VECTOR ( 'NONE', #4582, 1000.000000000000114 ) ;
#76756=CARTESIAN_POINT ( 'NONE',  ( -109.5222136401132502, -23.48786465467241769, 11.44779295918253759 ) ) ;
#76757=CARTESIAN_POINT ( 'NONE',  ( -14.54676392617323266, -15.37779485849079464, -1.500000000000002220 ) ) ;
#76759=CARTESIAN_POINT ( 'NONE',  ( -117.5222355478601060, -23.48783264082477729, -1.443836473390081254 ) ) ;
#76760=CARTESIAN_POINT ( 'NONE',  ( -42.62287095715004881, -29.50250243563736774, 8.947779886222148704 ) ) ;
#76761=CARTESIAN_POINT ( 'NONE',  ( -21.76810506448615712, 0.6044244127108716613, 11.49999999999998934 ) ) ;
#76765=CARTESIAN_POINT ( 'NONE',  ( -9.857415191643349672, 19.42730305858377449, -1.500000000000002220 ) ) ;
#76766=CARTESIAN_POINT ( 'NONE',  ( -71.70689869863497279, -25.24674333672842508, 6.146638408343236826 ) ) ;
#76769=CARTESIAN_POINT ( 'NONE',  ( -117.5228709571500758, -24.64898659630368272, 1.056161002820833028 ) ) ;
#76771=VERTEX_POINT ( 'NONE', #18909 ) ;
#76772=EDGE_CURVE ( 'NONE', #91650, #84010, #53069, .T. ) ;
#76773=ORIENTED_EDGE ( 'NONE', *, *, #52181, .T. ) ;
#76774=ORIENTED_EDGE ( 'NONE', *, *, #66550, .T. ) ;
#76776=CARTESIAN_POINT ( 'NONE',  ( 18.66760434907605060, -10.05535386721697222, 11.49999999999998934 ) ) ;
#76778=CARTESIAN_POINT ( 'NONE',  ( -95.62287095715005592, -24.99156045073393173, 7.747789690856161648 ) ) ;
#76781=CARTESIAN_POINT ( 'NONE',  ( -18.22047185089115828, 6.579378235550767506, -1.500000000000002220 ) ) ;
#76782=B_SPLINE_CURVE_WITH_KNOTS ( 'NONE', 3,
 ( #41847, #80392, #57073, #40825 ),
 .UNSPECIFIED., .F., .F.,
 ( 4, 4 ),
 ( 0.000000000000000000, 9.999999999997510880E-05 ),
 .UNSPECIFIED. ) ;
#76783=CARTESIAN_POINT ( 'NONE',  ( -70.29579152553412769, -25.31157247813958122, 5.315013286592739306 ) ) ;
#76785=CARTESIAN_POINT ( 'NONE',  ( -11.39837868854680814, -15.77482985264681403, 11.49999999999999645 ) ) ;
#76786=CARTESIAN_POINT ( 'NONE',  ( -42.52287095715006870, -23.95044443724991368, 10.65354141964649415 ) ) ;
#76787=EDGE_CURVE ( 'NONE', #5690, #63070, #73704, .T. ) ;
#76788=EDGE_CURVE ( 'NONE', #62952, #42367, #37133, .T. ) ;
#76790=ORIENTED_EDGE ( 'NONE', *, *, #41680, .F. ) ;
#76794=CARTESIAN_POINT ( 'NONE',  ( -91.62287095715002749, -23.95044443724991368, 10.65354141964649592 ) ) ;
#76795=CARTESIAN_POINT ( 'NONE',  ( -101.3738023147422638, -25.26303730729093999, 3.986250639247583827 ) ) ;
#76796=CARTESIAN_POINT ( 'NONE',  ( 19.40334540789412188, 3.064012487144803565, -1.500000000000002220 ) ) ;
#76797=AXIS2_PLACEMENT_3D ( 'NONE', #10868, #19964, #41833 ) ;
#76798=CARTESIAN_POINT ( 'NONE',  ( -41.44897309030830712, -25.27805984287601504, 4.366647756403065017 ) ) ;
#76799=EDGE_LOOP ( 'NONE', ( #74366, #48261, #792, #56333 ) ) ;
#76800=CARTESIAN_POINT ( 'NONE',  ( 5.689979955356517571, -20.79666814084963278, -1.500000000000002220 ) ) ;
#76801=CARTESIAN_POINT ( 'NONE',  ( -33.57506839788266007, -24.66019654487198665, 8.947790411086133489 ) ) ;
#76802=CARTESIAN_POINT ( 'NONE',  ( -74.22287095715006444, -23.47593901973090169, -1.443836447538997536 ) ) ;
#76803=CARTESIAN_POINT ( 'NONE',  ( -80.52287095715006160, -25.00158670708909625, 2.256160236439166411 ) ) ;
#76804=CARTESIAN_POINT ( 'NONE',  ( -1.973530150111237003, 22.95712487800313539, -1.500000000000002220 ) ) ;
#76806=EDGE_CURVE ( 'NONE', #24519, #33217, #77296, .T. ) ;
#76808=LINE ( 'NONE', #46380, #79096 ) ;
#76809=LINE ( 'NONE', #7308, #37709 ) ;
#76810=CARTESIAN_POINT ( 'NONE',  ( 5.087728227403598424, 19.53446797131710611, 11.49999999999999645 ) ) ;
#76811=CARTESIAN_POINT ( 'NONE',  ( -121.6234957283108145, -24.66019654487200441, 8.947790411086119278 ) ) ;
#76812=CARTESIAN_POINT ( 'NONE',  ( -101.7020366304713832, -25.16380645952672168, 6.919780044220484427 ) ) ;
#76813=CARTESIAN_POINT ( 'NONE',  ( -110.4629859055347936, -25.10921374666837735, 2.835693975498917663 ) ) ;
#76815=CARTESIAN_POINT ( 'NONE',  ( -110.9796143976588070, -25.18425627932603916, 3.502226522025594591 ) ) ;
#76816=CARTESIAN_POINT ( 'NONE',  ( 19.48829924427396421, 3.997931079995220127, 11.49999999999998934 ) ) ;
#76817=EDGE_CURVE ( 'NONE', #86369, #55468, #11902, .T. ) ;
#76819=CARTESIAN_POINT ( 'NONE',  ( 18.78060722631472501, -6.265068672152646734, -1.500000000000002220 ) ) ;
#76821=ADVANCED_FACE ( 'NONE', ( #5683 ), #46718, .T. ) ;
#76822=CARTESIAN_POINT ( 'NONE',  ( -39.73251464975087544, -25.10925631031845384, 3.010156874704200902 ) ) ;
#76824=CARTESIAN_POINT ( 'NONE',  ( -14.15296684469643118, 15.14645709676483420, 11.49999999999999645 ) ) ;
#76825=LINE ( 'NONE', #74842, #87240 ) ;
#76826=CARTESIAN_POINT ( 'NONE',  ( -50.26765004257320868, -25.31439277774918395, 5.200244519690546241 ) ) ;
#76827=CARTESIAN_POINT ( 'NONE',  ( -18.45961786539058380, -13.25243217869837231, 11.49999999999999645 ) ) ;
#76828=ORIENTED_EDGE ( 'NONE', *, *, #17885, .F. ) ;
#76830=B_SPLINE_CURVE_WITH_KNOTS ( 'NONE', 3,
 ( #44853, #14376, #76274, #46337 ),
 .UNSPECIFIED., .F., .F.,
 ( 4, 4 ),
 ( 1.387778780781445676E-17, 0.0001000000000000028508 ),
 .UNSPECIFIED. ) ;
#76832=CARTESIAN_POINT ( 'NONE',  ( -19.98115086844608612, 2.773124471107000666, 11.49999999999998934 ) ) ;
#76836=VERTEX_POINT ( 'NONE', #76181 ) ;
#76837=CARTESIAN_POINT ( 'NONE',  ( -73.52287095715007581, -24.65952944569304606, 1.056160979905697239 ) ) ;
#76838=CARTESIAN_POINT ( 'NONE',  ( -13.69284064830502423, 18.33895024417757469, -1.500000000000002220 ) ) ;
#76839=CARTESIAN_POINT ( 'NONE',  ( -50.97853604095990221, -25.18439684119721278, 3.451784566745564664 ) ) ;
#76840=CARTESIAN_POINT ( 'NONE',  ( -6.031157642910047301, -20.80930661755759203, -1.500000000000002220 ) ) ;
#76841=CARTESIAN_POINT ( 'NONE',  ( -90.62287095715004170, -29.50250243563736774, 8.947779886222139822 ) ) ;
#76843=CARTESIAN_POINT ( 'NONE',  ( -0.7727808018759799724, -20.89725122839497828, 11.49999999999999645 ) ) ;
#76844=ORIENTED_EDGE ( 'NONE', *, *, #96170, .F. ) ;
#76845=CARTESIAN_POINT ( 'NONE',  ( -124.6256202920364586, -23.73766607897671577, -1.055555164236449572 ) ) ;
#76846=CARTESIAN_POINT ( 'NONE',  ( -18.24146354680218707, 12.35505607031776165, 11.49999999999998934 ) ) ;
#76847=VECTOR ( 'NONE', #14186, 1000.000000000000114 ) ;
#76849=CARTESIAN_POINT ( 'NONE',  ( -40.43756433397305727, -25.29087034402937206, 2.832404424902956297 ) ) ;
#76850=ADVANCED_FACE ( 'NONE', ( #91409 ), #21887, .T. ) ;
#76851=ORIENTED_EDGE ( 'NONE', *, *, #37851, .F. ) ;
#76853=FACE_OUTER_BOUND ( 'NONE', #78117, .T. ) ;
#76854=ADVANCED_FACE ( 'NONE', ( #51873 ), #77470, .T. ) ;
#76856=CARTESIAN_POINT ( 'NONE',  ( -72.58424668660525469, -24.51419770103156281, 9.386484678747185839 ) ) ;
#76857=VERTEX_POINT ( 'NONE', #62997 ) ;
#76858=VERTEX_POINT ( 'NONE', #33031 ) ;
#76859=CARTESIAN_POINT ( 'NONE',  ( -71.58081214425558869, -24.66019654487199730, 8.947790411086113949 ) ) ;
#76860=DIRECTION ( 'NONE',  ( -3.773278334453079030E-23, 0.9999999999976377785, 2.173523156925979128E-06 ) ) ;
#76862=CARTESIAN_POINT ( 'NONE',  ( -11.47117155886032158, -16.94740806926979815, -1.500000000000002220 ) ) ;
#76868=CARTESIAN_POINT ( 'NONE',  ( 10.93216147639808611, 19.43004700418156361, -1.500000000000002220 ) ) ;
#76871=VERTEX_POINT ( 'NONE', #17807 ) ;
#76873=CARTESIAN_POINT ( 'NONE',  ( -29.21927636257191807, -24.63645895185818802, 7.471892006582644186 ) ) ;
#76874=CARTESIAN_POINT ( 'NONE',  ( -18.54028579900546703, -9.471972883075929772, -1.500000000000002220 ) ) ;
#76875=VERTEX_POINT ( 'NONE', #25413 ) ;
#76879=LINE ( 'NONE', #15991, #98922 ) ;
#76882=PLANE ( 'NONE',  #43005 ) ;
#76883=CARTESIAN_POINT ( 'NONE',  ( -80.62287095715005592, -24.99156045073393173, 7.747789690856161648 ) ) ;
#76885=EDGE_CURVE ( 'NONE', #79998, #59480, #13146, .T. ) ;
#76886=CARTESIAN_POINT ( 'NONE',  ( -40.62287095715004170, -25.00182538069145011, 7.747789668545099317 ) ) ;
#76887=B_SPLINE_CURVE_WITH_KNOTS ( 'NONE', 3,
 ( #87615, #49063, #18098, #79991, #10479, #31781 ),
 .UNSPECIFIED., .F., .F.,
 ( 4, 2, 4 ),
 ( 1.570755371633993761E-05, 0.001396183895866089271, 0.002776660238015838614 ),
 .UNSPECIFIED. ) ;
#76888=CARTESIAN_POINT ( 'NONE',  ( -109.4786293639607493, -25.16483953145740671, 3.092510198109223118 ) ) ;
#76890=CARTESIAN_POINT ( 'NONE',  ( -2.513997614918375589, -22.02279109229760223, 11.49999999999999645 ) ) ;
#76891=ORIENTED_EDGE ( 'NONE', *, *, #94325, .T. ) ;
#76894=CARTESIAN_POINT ( 'NONE',  ( 14.74224262856723833, 17.19160420931263999, -1.500000000000002220 ) ) ;
#76896=EDGE_CURVE ( 'NONE', #79893, #3121, #50737, .T. ) ;
#76897=ADVANCED_FACE ( 'NONE', ( #92909 ), #79695, .F. ) ;
#76898=CARTESIAN_POINT ( 'NONE',  ( -92.52287095715006160, -24.65952944569304606, 1.056160979905700570 ) ) ;
#76899=ORIENTED_EDGE ( 'NONE', *, *, #44272, .F. ) ;
#76900=ORIENTED_EDGE ( 'NONE', *, *, #31509, .T. ) ;
#76904=B_SPLINE_CURVE_WITH_KNOTS ( 'NONE', 3,
 ( #57093, #48970, #8896, #3312, #55084, #32729 ),
 .UNSPECIFIED., .F., .F.,
 ( 4, 2, 4 ),
 ( 0.000000000000000000, 0.001380901958385389412, 0.002761803916770778824 ),
 .UNSPECIFIED. ) ;
#76905=B_SPLINE_CURVE_WITH_KNOTS ( 'NONE', 3,
 ( #43462, #57690, #49580, #89131, #35839, #11997, #74396, #57203, #80513, #10498, #4400, #97239, #35348, #96735, #19604, #80011, #50565, #66810 ),
 .UNSPECIFIED., .F., .F.,
 ( 4, 2, 2, 2, 2, 2, 2, 2, 4 ),
 ( 0.000000000000000000, 0.0002684257652534861004, 0.0005368515305069722007, 0.0008052772957604583011, 0.001073703061013944401, 0.001342128826267430502, 0.001610554591520916602, 0.001878980356774402703, 0.002147406122027888803 ),
 .UNSPECIFIED. ) ;
#76906=CARTESIAN_POINT ( 'NONE',  ( -13.04681709000290013, -15.30929823114697541, 11.49999999999998934 ) ) ;
#76907=B_SPLINE_SURFACE_WITH_KNOTS ( 'NONE', 3, 3, ( 
 ( #19600, #56699, #81014, #87630 ),
 ( #18114, #80007, #10495, #41968 ),
 ( #41455, #72413, #33836, #42470 ),
 ( #64824, #88632, #18601, #49577 ),
 ( #96243, #26727, #57687, #19101 ),
 ( #73409, #3903, #65811, #96731 ),
 ( #5877, #98720, #29715, #36838 ) ),
 .UNSPECIFIED., .F., .F., .F.,
 ( 4, 3, 4 ),
 ( 4, 4 ),
 ( 0.7945040050992234759, 0.8970133687736496775, 0.9995227324480758790 ),
 ( 0.2595599550269429012, 0.2606925096813342280 ),
 .UNSPECIFIED. ) ;
#76908=CARTESIAN_POINT ( 'NONE',  ( -88.58953762381671027, -23.48783264082479150, -1.443836473390063935 ) ) ;
#76909=VERTEX_POINT ( 'NONE', #569 ) ;
#76910=FACE_OUTER_BOUND ( 'NONE', #65180, .T. ) ;
#76911=CARTESIAN_POINT ( 'NONE',  ( 16.92800457317958518, -14.60656088873787262, -1.500000000000002220 ) ) ;
#76916=CARTESIAN_POINT ( 'NONE',  ( -101.3540785649959304, -25.16257400088798235, 6.680569373907164099 ) ) ;
#76917=PLANE ( 'NONE',  #26458 ) ;
#76919=CARTESIAN_POINT ( 'NONE',  ( -68.52287095715006160, -24.66019654487199730, 8.947790411086124607 ) ) ;
#76921=CARTESIAN_POINT ( 'NONE',  ( 12.76379665850700640, 14.79237594083867080, 11.49999999999998934 ) ) ;
#76922=CARTESIAN_POINT ( 'NONE',  ( -33.55620429048341435, -24.64898659630528144, 1.056161002820815931 ) ) ;
#76923=CARTESIAN_POINT ( 'NONE',  ( -2.231587876719630437, -21.34735720706076378, -1.500000000000002220 ) ) ;
#76927=CARTESIAN_POINT ( 'NONE',  ( 17.70901601935662839, 14.43836031950349152, -1.500000000000002220 ) ) ;
#76928=VECTOR ( 'NONE', #30293, 1000.000000000000114 ) ;
#76932=CARTESIAN_POINT ( 'NONE',  ( -96.55782220809594207, -23.73791477778912196, 11.05961554403170410 ) ) ;
#76934=CARTESIAN_POINT ( 'NONE',  ( 8.743921044546416610, -18.04861246754477477, 11.49999999999999645 ) ) ;
#76935=CARTESIAN_POINT ( 'NONE',  ( -80.06557898417501917, -25.26612378837472761, 4.529242823862608347 ) ) ;
#76938=PLANE ( 'NONE',  #27803 ) ;
#76940=CARTESIAN_POINT ( 'NONE',  ( -109.5228709571500616, -24.33832256527048088, 0.1851278514138657294 ) ) ;
#76944=CARTESIAN_POINT ( 'NONE',  ( 6.244050601037331560, 20.82503750550150912, -1.500000000000002220 ) ) ;
#76945=CARTESIAN_POINT ( 'NONE',  ( -117.6228709571500559, -23.48783264082479505, -1.443836473390058384 ) ) ;
#76946=CARTESIAN_POINT ( 'NONE',  ( 18.24213732562919787, -7.162457363581539838, -1.500000000000002220 ) ) ;
#76947=CARTESIAN_POINT ( 'NONE',  ( -29.62287095715004881, -29.50248528299834305, 1.056150588822498460 ) ) ;
#76948=ADVANCED_FACE ( 'NONE', ( #20280 ), #57886, .T. ) ;
#76949=B_SPLINE_CURVE_WITH_KNOTS ( 'NONE', 3,
 ( #2741, #35184, #49924, #81353 ),
 .UNSPECIFIED., .F., .F.,
 ( 4, 4 ),
 ( 0.3189916387590558400, 0.3199923857998208110 ),
 .UNSPECIFIED. ) ;
#76953=CARTESIAN_POINT ( 'NONE',  ( -91.58852088267255454, -24.35071581493543391, 9.817618358456023486 ) ) ;
#76955=CARTESIAN_POINT ( 'NONE',  ( 19.18951349294833264, 7.196795126939715459, 11.49999999999999645 ) ) ;
#76956=CARTESIAN_POINT ( 'NONE',  ( -39.11368603858827697, -25.31200071491427650, 4.685369829760536398 ) ) ;
#76957=CARTESIAN_POINT ( 'NONE',  ( -120.5579443694568909, -23.48783264082477018, -1.443836473390085695 ) ) ;
#76958=EDGE_CURVE ( 'NONE', #19118, #28096, #73724, .T. ) ;
#76959=ORIENTED_EDGE ( 'NONE', *, *, #11779, .F. ) ;
#76961=CARTESIAN_POINT ( 'NONE',  ( -109.5228709571500616, -29.50248528299804818, 1.056150453629043584 ) ) ;
#76963=CARTESIAN_POINT ( 'NONE',  ( -125.5547320878391275, -24.63419186844610920, 9.035850630976920428 ) ) ;
#76965=CARTESIAN_POINT ( 'NONE',  ( -110.5228709571500616, -23.48786465467242479, 11.44779295918253936 ) ) ;
#76967=CARTESIAN_POINT ( 'NONE',  ( -18.41700849636773540, 13.91914711744011157, 11.49999999999999645 ) ) ;
#76968=CARTESIAN_POINT ( 'NONE',  ( -16.48365427610503886, -15.78576583860491489, -1.500000000000002220 ) ) ;
#76969=DIRECTION ( 'NONE',  ( -7.150924204855701834E-40, -2.173523156925979975E-06, 0.9999999999976378895 ) ) ;
#76971=CARTESIAN_POINT ( 'NONE',  ( -85.52287095715004739, -24.99156044556120193, 7.747789690856173195 ) ) ;
#76972=AXIS2_PLACEMENT_3D ( 'NONE', #19927, #18930, #80843 ) ;
#76973=CARTESIAN_POINT ( 'NONE',  ( -12.73782554413503654, -18.45060914899308457, 11.49999999999999645 ) ) ;
#76976=CARTESIAN_POINT ( 'NONE',  ( -43.66333338684359688, -23.48783264082478084, -1.443836473390076369 ) ) ;
#76977=CARTESIAN_POINT ( 'NONE',  ( -19.93956527825925917, 9.129326121205059152, -1.500000000000002220 ) ) ;
#76979=DIRECTION ( 'NONE',  ( -3.773278334453079618E-23, 0.9999999999976377785, 2.173523156925978705E-06 ) ) ;
#76980=CARTESIAN_POINT ( 'NONE',  ( -104.5480626255145040, -24.65952944569304606, 1.056160979905702346 ) ) ;
#76982=CARTESIAN_POINT ( 'NONE',  ( -103.5228709571500758, -24.65952944569304606, 1.056160979905702346 ) ) ;
#76983=ORIENTED_EDGE ( 'NONE', *, *, #8238, .T. ) ;
#76984=CARTESIAN_POINT ( 'NONE',  ( -20.02755620033356010, -4.236777897013602079, -1.500000000000002220 ) ) ;
#76985=EDGE_LOOP ( 'NONE', ( #14839, #7233, #98763, #89657 ) ) ;
#76986=B_SPLINE_CURVE_WITH_KNOTS ( 'NONE', 3,
 ( #59920, #81242, #80750, #19338, #42210, #59405, #35076, #19825, #35578, #66554, #97947, #4627 ),
 .UNSPECIFIED., .F., .F.,
 ( 4, 2, 2, 2, 2, 4 ),
 ( 0.000000000000000000, 0.0001492647388655131511, 0.0002985294777310263021, 0.0005970589554620495685, 0.0008955884331930726722, 0.001194117910924095884 ),
 .UNSPECIFIED. ) ;
#76988=ORIENTED_EDGE ( 'NONE', *, *, #30426, .T. ) ;
#76990=CARTESIAN_POINT ( 'NONE',  ( -22.28253579152010033, 6.022996098971622914, 11.49999999999998934 ) ) ;
#76991=CARTESIAN_POINT ( 'NONE',  ( -82.52287095715006160, -24.64898659630367916, 1.056161002820826145 ) ) ;
#76992=CARTESIAN_POINT ( 'NONE',  ( -14.66855384320708033, -14.05595220846724835, -1.500000000000002220 ) ) ;
#76993=ORIENTED_EDGE ( 'NONE', *, *, #45664, .F. ) ;
#76994=CARTESIAN_POINT ( 'NONE',  ( -26.07725539581784346, -24.96266517532310303, 5.848370260082334404 ) ) ;
#76995=CARTESIAN_POINT ( 'NONE',  ( -83.52287095715006160, -29.50250786944525672, 11.44777988621623521 ) ) ;
#76996=CARTESIAN_POINT ( 'NONE',  ( -101.2401810617817262, -25.17942323519604386, 6.818125126578213013 ) ) ;
#76997=DIRECTION ( 'NONE',  ( 0.000000000000000000, -2.173523156925980399E-06, 0.9999999999976378895 ) ) ;
#76998=CARTESIAN_POINT ( 'NONE',  ( -19.34459864454321831, 9.218434461607088792, 11.49999999999999645 ) ) ;
#77001=CARTESIAN_POINT ( 'NONE',  ( -61.54846442012016894, -24.15620529776627734, 10.23563542870660825 ) ) ;
#77002=EDGE_LOOP ( 'NONE', ( #53234, #38636, #49107, #70273 ) ) ;
#77003=CARTESIAN_POINT ( 'NONE',  ( 20.68991284688621946, 0.5745778482356619365, 11.49999999999998934 ) ) ;
#77006=CARTESIAN_POINT ( 'NONE',  ( -123.6228709571500417, -23.73907113216991149, -1.053371485793226592 ) ) ;
#77008=EDGE_CURVE ( 'NONE', #84073, #71576, #58377, .T. ) ;
#77012=EDGE_CURVE ( 'NONE', #71187, #69320, #45872, .T. ) ;
#77013=CARTESIAN_POINT ( 'NONE',  ( -55.52287095715004739, -24.14406661686757261, 10.28769366194082302 ) ) ;
#77014=DIRECTION ( 'NONE',  ( 0.000000000000000000, 0.9999999999976377785, 2.173523156925979128E-06 ) ) ;
#77015=CARTESIAN_POINT ( 'NONE',  ( -65.57704652348438401, -25.00158670708910691, 2.256160236439222366 ) ) ;
#77016=CARTESIAN_POINT ( 'NONE',  ( 15.04091035147580335, -15.99806323810862274, 11.49999999999999645 ) ) ;
#77018=EDGE_CURVE ( 'NONE', #20503, #15484, #76043, .T. ) ;
#77019=CARTESIAN_POINT ( 'NONE',  ( -89.51458554710613669, -23.96169478059713498, 10.65365249895717703 ) ) ;
#77020=CARTESIAN_POINT ( 'NONE',  ( -3.649967738973055376, -22.27025559232234642, 11.49999999999998934 ) ) ;
#77021=EDGE_CURVE ( 'NONE', #41820, #64103, #41654, .T. ) ;
#77022=AXIS2_PLACEMENT_3D ( 'NONE', #17474, #84983, #7355 ) ;
#77023=CARTESIAN_POINT ( 'NONE',  ( -20.92093621315066443, -1.481899440790641842, 11.49999999999998934 ) ) ;
#77024=CARTESIAN_POINT ( 'NONE',  ( -111.5562042904833930, -24.64898659630529565, 1.056161002820831918 ) ) ;
#77031=CARTESIAN_POINT ( 'NONE',  ( -59.62287095715004170, -24.50321055353805377, 9.387540953477532923 ) ) ;
#77032=CARTESIAN_POINT ( 'NONE',  ( 18.54456287915894563, -10.88813254144886322, -1.500000000000002220 ) ) ;
#77035=CARTESIAN_POINT ( 'NONE',  ( 1.943494986365726485, -21.02143711168614004, 11.49999999999998934 ) ) ;
#77037=CARTESIAN_POINT ( 'NONE',  ( -61.66538019323460418, -25.14083923594472125, 2.947789366366679875 ) ) ;
#77038=FACE_OUTER_BOUND ( 'NONE', #67047, .T. ) ;
#77039=DIRECTION ( 'NONE',  ( -3.773278334453079030E-23, 0.9999999999976377785, 2.173523156925979128E-06 ) ) ;
#77041=CARTESIAN_POINT ( 'NONE',  ( -5.843409716339609261, -21.38298466452703650, -1.500000000000002220 ) ) ;
#77042=CARTESIAN_POINT ( 'NONE',  ( -81.51308774969011495, -23.96169478059713143, 10.65365249895718591 ) ) ;
#77044=ORIENTED_EDGE ( 'NONE', *, *, #83004, .F. ) ;
#77045=CARTESIAN_POINT ( 'NONE',  ( -51.15602047325173629, -25.24860005136912733, 4.998863007599903874 ) ) ;
#77049=ADVANCED_FACE ( 'NONE', ( #81703 ), #65009, .T. ) ;
#77050=CARTESIAN_POINT ( 'NONE',  ( 8.422564666779264186, -17.53554878399664574, -1.500000000000002220 ) ) ;
#77051=VECTOR ( 'NONE', #66779, 1000.000000000000114 ) ;
#77052=CARTESIAN_POINT ( 'NONE',  ( -21.27170209485220198, -2.091907790468015005, 11.49999999999998934 ) ) ;
#77053=CARTESIAN_POINT ( 'NONE',  ( -62.58763761694054040, -24.34968618360933945, 0.1864209137778799485 ) ) ;
#77055=CARTESIAN_POINT ( 'NONE',  ( -110.9353407762807393, -25.05712135967895549, 7.447789548357303779 ) ) ;
#77056=CARTESIAN_POINT ( 'NONE',  ( -100.4839344043725333, -25.27359974982199020, 3.295731817984544509 ) ) ;
#77057=CARTESIAN_POINT ( 'NONE',  ( -10.65177407370799045, -20.06881281718593613, -1.500000000000002220 ) ) ;
#77058=CARTESIAN_POINT ( 'NONE',  ( -98.55771462834329100, -23.73766607897669800, -1.055555164236454013 ) ) ;
#77060=CARTESIAN_POINT ( 'NONE',  ( -19.19514693104756375, 4.742496307885142315, 11.49999999999999645 ) ) ;
#77061=CARTESIAN_POINT ( 'NONE',  ( -115.6228709571500559, -23.47596703998600631, 11.44779298504227860 ) ) ;
#77062=ORIENTED_EDGE ( 'NONE', *, *, #51370, .F. ) ;
#77063=CARTESIAN_POINT ( 'NONE',  ( -60.52287095715006160, -25.00158670708908915, 2.256160236439166411 ) ) ;
#77064=CARTESIAN_POINT ( 'NONE',  ( -80.52287095715006160, -23.84081130425359163, 10.88220057483156644 ) ) ;
#77065=CARTESIAN_POINT ( 'NONE',  ( -68.52287095715001897, -24.34917612406836795, 0.1852690917426542405 ) ) ;
#77066=CARTESIAN_POINT ( 'NONE',  ( 21.13687465659472409, 4.681744431724916389, -1.500000000000002220 ) ) ;
#77068=CARTESIAN_POINT ( 'NONE',  ( -19.08929872761019908, -3.557156390981079053, -1.500000000000002220 ) ) ;
#77069=CARTESIAN_POINT ( 'NONE',  ( -80.52287095715006160, -23.85229601348996908, 10.88205029486208986 ) ) ;
#77071=EDGE_CURVE ( 'NONE', #94542, #16286, #66377, .T. ) ;
#77072=CARTESIAN_POINT ( 'NONE',  ( 9.833179757865110560, 17.22857952739193266, -1.500000000000002220 ) ) ;
#77074=CARTESIAN_POINT ( 'NONE',  ( 0.7445296356392017145, -20.29553345556499622, 11.49999999999999645 ) ) ;
#77075=CARTESIAN_POINT ( 'NONE',  ( -80.53951533976572819, -24.83618233451450408, 1.606449574219532384 ) ) ;
#77079=B_SPLINE_CURVE_WITH_KNOTS ( 'NONE', 3,
 ( #86718, #92825, #31941, #23307, #85724, #17208, #54292, #39048 ),
 .UNSPECIFIED., .F., .F.,
 ( 4, 2, 2, 4 ),
 ( 6.384118678605199737E-06, 0.002007151183507247146, 0.003007534715921569932, 0.004007918248335893587 ),
 .UNSPECIFIED. ) ;
#77080=ORIENTED_EDGE ( 'NONE', *, *, #38645, .T. ) ;
#77081=CARTESIAN_POINT ( 'NONE',  ( -0.08079981110223319329, -22.00398294951504496, 0.01136689895587368430 ) ) ;
#77082=CARTESIAN_POINT ( 'NONE',  ( -92.52287095715009002, -23.72747288104470087, -1.053458166803225460 ) ) ;
#77085=CARTESIAN_POINT ( 'NONE',  ( -40.62644180606930888, -24.92592662359561118, 8.075495903017996469 ) ) ;
#77088=CARTESIAN_POINT ( 'NONE',  ( -19.91332876899582160, 2.521106391696132931, 11.49999999999998934 ) ) ;
#77090=CARTESIAN_POINT ( 'NONE',  ( -85.52287095715013265, -24.91544648472627088, 1.928969306349433310 ) ) ;
#77092=CARTESIAN_POINT ( 'NONE',  ( -130.5728709571500588, -23.56000036390797092, -1.497999999999531040 ) ) ;
#77094=CARTESIAN_POINT ( 'NONE',  ( -4.124250913864588419, 22.51598698906299845, 11.49999999999999645 ) ) ;
#77095=CARTESIAN_POINT ( 'NONE',  ( -5.793434319722853054, -21.96748078227757617, -1.500000000000002220 ) ) ;
#77098=CARTESIAN_POINT ( 'NONE',  ( -57.62287095715004881, -29.50248528299804818, 1.056150453629034924 ) ) ;
#77100=CARTESIAN_POINT ( 'NONE',  ( -73.58953762381672448, -23.48783264082478084, -1.443836473390067487 ) ) ;
#77102=PLANE ( 'NONE',  #61518 ) ;
#77104=CARTESIAN_POINT ( 'NONE',  ( -5.548086588741434788, -19.59138962566686004, -1.500000000000002220 ) ) ;
#77106=CARTESIAN_POINT ( 'NONE',  ( 8.272623322502495213, 21.45567517505680044, -1.500000000000002220 ) ) ;
#77107=CARTESIAN_POINT ( 'NONE',  ( -54.52206316579233203, -23.48786465467240703, 11.44779295918255180 ) ) ;
#77108=ORIENTED_EDGE ( 'NONE', *, *, #40256, .F. ) ;
#77109=CARTESIAN_POINT ( 'NONE',  ( -108.5535921372889163, -24.15620529776629510, 10.23563542870659404 ) ) ;
#77111=CARTESIAN_POINT ( 'NONE',  ( -40.62287095715006302, -23.84047902841600930, -0.8780736468305813114 ) ) ;
#77112=CARTESIAN_POINT ( 'NONE',  ( 6.411417644607832145, 20.24884965431308714, 11.49999999999999645 ) ) ;
#77114=EDGE_LOOP ( 'NONE', ( #9866, #53449, #95509, #92838 ) ) ;
#77115=CARTESIAN_POINT ( 'NONE',  ( 4.265775719338400052, 21.77767432286298543, 11.49999999999998934 ) ) ;
#77116=B_SPLINE_CURVE_WITH_KNOTS ( 'NONE', 3,
 ( #80993, #74860, #51551, #73388 ),
 .UNSPECIFIED., .F., .F.,
 ( 4, 4 ),
 ( 0.000000000000000000, 9.999999999998206125E-05 ),
 .UNSPECIFIED. ) ;
#77117=CARTESIAN_POINT ( 'NONE',  ( -20.24099117049231467, 3.958469829285517161, 11.49999999999998934 ) ) ;
#77120=EDGE_CURVE ( 'NONE', #21700, #89515, #42107, .T. ) ;
#77121=CARTESIAN_POINT ( 'NONE',  ( -108.9610644980590450, -25.31627158989577353, 4.357072244912905568 ) ) ;
#77123=VERTEX_POINT ( 'NONE', #38017 ) ;
#77125=CARTESIAN_POINT ( 'NONE',  ( -91.54879471971332805, -24.34968618360934300, 0.1864209137778843617 ) ) ;
#77126=ORIENTED_EDGE ( 'NONE', *, *, #52858, .T. ) ;
#77127=CARTESIAN_POINT ( 'NONE',  ( -121.5895376238167387, -23.47596703998600631, 11.44779298504227683 ) ) ;
#77129=CARTESIAN_POINT ( 'NONE',  ( 15.20108283357335921, -14.20388156210760577, -1.500000000000002220 ) ) ;
#77130=CARTESIAN_POINT ( 'NONE',  ( -21.42251255223715134, 3.917230396363152067, 11.49999999999999645 ) ) ;
#77133=CARTESIAN_POINT ( 'NONE',  ( -99.10821524085508827, -25.16307519314475982, 6.860273405324268658 ) ) ;
#77134=CARTESIAN_POINT ( 'NONE',  ( -1.649324495273077451, -22.40575143947253167, 11.49999999999998934 ) ) ;
#77135=EDGE_CURVE ( 'NONE', #1913, #16500, #28399, .T. ) ;
#77136=VECTOR ( 'NONE', #80463, 1000.000000000000114 ) ;
#77138=EDGE_LOOP ( 'NONE', ( #778, #25874, #8448, #67361 ) ) ;
#77139=CARTESIAN_POINT ( 'NONE',  ( -50.52287095715008292, -24.92604778743017491, 8.074972756849357225 ) ) ;
#77141=EDGE_CURVE ( 'NONE', #98958, #56064, #15173, .T. ) ;
#77142=EDGE_LOOP ( 'NONE', ( #69774, #8385, #6756, #2548 ) ) ;
#77147=CARTESIAN_POINT ( 'NONE',  ( -13.85510387911049079, -16.26762222697724880, -1.500000000000002220 ) ) ;
#77148=EDGE_LOOP ( 'NONE', ( #78390, #66600, #91251, #48963 ) ) ;
#77149=CARTESIAN_POINT ( 'NONE',  ( -5.295558097854481616, 20.35707381486366785, -1.500000000000002220 ) ) ;
#77150=CARTESIAN_POINT ( 'NONE',  ( -30.44149352667901809, -24.26500045891999946, 0.04395666736089841320 ) ) ;
#77153=CARTESIAN_POINT ( 'NONE',  ( -37.62287095715005592, -29.50248528299804818, 1.056150453629031594 ) ) ;
#77154=CARTESIAN_POINT ( 'NONE',  ( 4.628415685485613551, -21.52068878818806752, -1.500000000000002220 ) ) ;
#77156=VERTEX_POINT ( 'NONE', #45144 ) ;
#77157=LINE ( 'NONE', #61960, #3287 ) ;
#77158=VECTOR ( 'NONE', #96535, 1000.000000000000114 ) ;
#77159=CARTESIAN_POINT ( 'NONE',  ( -107.5895376238167529, -23.47593901973091235, -1.443836447538999312 ) ) ;
#77160=VECTOR ( 'NONE', #17583, 1000.000000000000114 ) ;
#77164=CARTESIAN_POINT ( 'NONE',  ( 17.95810460983813783, 11.44545274529666479, 11.49999999999998934 ) ) ;
#77166=CARTESIAN_POINT ( 'NONE',  ( -107.6297665980143137, -23.96169478059713853, 10.65365249895717348 ) ) ;
#77167=LINE ( 'NONE', #15778, #84 ) ;
#77169=CARTESIAN_POINT ( 'NONE',  ( 14.28312119630281174, -17.39864199977734671, -1.500000000000002220 ) ) ;
#77170=CARTESIAN_POINT ( 'NONE',  ( -108.8785801883210951, -25.06174035403189038, 7.474877196992075312 ) ) ;
#77171=VERTEX_POINT ( 'NONE', #59874 ) ;
#77173=CARTESIAN_POINT ( 'NONE',  ( 0.6594449095415070294, 19.62168050102039629, 11.49999999999999645 ) ) ;
#77175=CARTESIAN_POINT ( 'NONE',  ( -100.6228709571500701, -24.82576562982393042, 8.398263435472967942 ) ) ;
#77177=CARTESIAN_POINT ( 'NONE',  ( -68.93918693012690824, -25.24795196732124936, 6.184868460502651821 ) ) ;
#77178=DIRECTION ( 'NONE',  ( -3.773278334453079030E-23, 0.9999999999976377785, 2.173523156925979128E-06 ) ) ;
#77179=CARTESIAN_POINT ( 'NONE',  ( -91.96414918007445749, -25.30572777988224331, 5.920366768842380445 ) ) ;
#77180=AXIS2_PLACEMENT_3D ( 'NONE', #6896, #54576, #85512 ) ;
#77181=CARTESIAN_POINT ( 'NONE',  ( 7.891737972721761807, -18.10977644326358771, -1.500000000000002220 ) ) ;
#77182=VERTEX_POINT ( 'NONE', #59365 ) ;
#77183=CARTESIAN_POINT ( 'NONE',  ( -120.5228709571501184, -24.92604778743018556, 8.074972756849353672 ) ) ;
#77184=CARTESIAN_POINT ( 'NONE',  ( -70.62287095715005592, -25.00158670708909270, 2.256160236439166855 ) ) ;
#77185=EDGE_CURVE ( 'NONE', #26377, #52082, #51756, .T. ) ;
#77187=EDGE_CURVE ( 'NONE', #28708, #23124, #63864, .T. ) ;
#77188=ORIENTED_EDGE ( 'NONE', *, *, #65059, .T. ) ;
#77189=CARTESIAN_POINT ( 'NONE',  ( -109.6228709571500417, -23.48786465467242124, 11.44779295918253936 ) ) ;
#77191=CARTESIAN_POINT ( 'NONE',  ( -90.52287095715006160, -23.48786465467241769, 11.44779295918254292 ) ) ;
#77192=CARTESIAN_POINT ( 'NONE',  ( -99.65618967412262919, -25.03145138608062226, 7.377943801491970710 ) ) ;
#77194=B_SPLINE_CURVE_WITH_KNOTS ( 'NONE', 3,
 ( #65422, #49188, #88236, #50667, #27328, #11592 ),
 .UNSPECIFIED., .F., .F.,
 ( 4, 2, 4 ),
 ( 6.384118695050191095E-06, 0.001386860460836595839, 0.002767336802978141459 ),
 .UNSPECIFIED. ) ;
#77195=CARTESIAN_POINT ( 'NONE',  ( -56.52287095715006870, -24.65952944569304606, 1.056160979905695463 ) ) ;
#77196=CARTESIAN_POINT ( 'NONE',  ( 19.86680303116296287, 2.261939200664708327, 11.49999999999998934 ) ) ;
#77197=CARTESIAN_POINT ( 'NONE',  ( -127.6228709571500559, -24.50216790748099882, 0.6166512839513782485 ) ) ;
#77198=CARTESIAN_POINT ( 'NONE',  ( -51.37986311123607663, -25.31231099970419862, 4.713062901810517680 ) ) ;
#77199=ORIENTED_EDGE ( 'NONE', *, *, #23551, .T. ) ;
#77202=CARTESIAN_POINT ( 'NONE',  ( -73.62287095715007013, -23.47596703998600276, 11.44779298504227860 ) ) ;
#77203=CARTESIAN_POINT ( 'NONE',  ( -35.57451790842697648, -23.48783264082477729, -1.443836473390077479 ) ) ;
#77204=CARTESIAN_POINT ( 'NONE',  ( -28.62287095715005947, -24.36053554431182988, 9.387565063642748342 ) ) ;
#77206=DIRECTION ( 'NONE',  ( -3.773278334444166432E-23, 1.000000000000000000, 0.000000000000000000 ) ) ;
#77207=CARTESIAN_POINT ( 'NONE',  ( -83.51756576996206149, -23.73766607897670511, -1.055555164236456900 ) ) ;
#77208=VECTOR ( 'NONE', #40144, 1000.000000000000114 ) ;
#77209=CARTESIAN_POINT ( 'NONE',  ( -47.62287095715004881, -29.50248528299804818, 1.056150453629033370 ) ) ;
#77214=CARTESIAN_POINT ( 'NONE',  ( -15.67655817637044890, 12.86142704545212290, -1.500000000000002220 ) ) ;
#77216=AXIS2_PLACEMENT_3D ( 'NONE', #65899, #89710, #2989 ) ;
#77217=CARTESIAN_POINT ( 'NONE',  ( -90.52287095715004739, -24.14321612903117753, -0.2833117244520893530 ) ) ;
#77218=ORIENTED_EDGE ( 'NONE', *, *, #86319, .F. ) ;
#77220=CARTESIAN_POINT ( 'NONE',  ( 19.93115673323400117, -2.579441489355707606, -1.500000000000002220 ) ) ;
#77221=CARTESIAN_POINT ( 'NONE',  ( 20.77832821955112408, -3.674247523096572099, 11.49999999999999645 ) ) ;
#77222=CARTESIAN_POINT ( 'NONE',  ( -15.83042281971428977, -15.45127431894796466, -1.500000000000002220 ) ) ;
#77223=CARTESIAN_POINT ( 'NONE',  ( -4.863915844574979275, 19.94883092034378791, -1.500000000000002220 ) ) ;
#77226=EDGE_LOOP ( 'NONE', ( #17707, #50253, #24219, #64712 ) ) ;
#77227=FACE_OUTER_BOUND ( 'NONE', #21332, .T. ) ;
#77230=CARTESIAN_POINT ( 'NONE',  ( -85.62287095715007013, -24.92604778743018201, 8.074972756849359001 ) ) ;
#77232=EDGE_CURVE ( 'NONE', #66603, #81403, #50532, .T. ) ;
#77233=VERTEX_POINT ( 'NONE', #44140 ) ;
#77234=EDGE_LOOP ( 'NONE', ( #890, #49369, #83141, #230 ) ) ;
#77236=CARTESIAN_POINT ( 'NONE',  ( -63.62287095715004881, -24.65952944569303895, 1.056160979905696129 ) ) ;
#77237=CARTESIAN_POINT ( 'NONE',  ( -68.49730927663665625, -24.51419770103157347, 9.386484678747180510 ) ) ;
#77238=CARTESIAN_POINT ( 'NONE',  ( -16.38011734009650411, 12.53836025512309149, -1.500000000000002220 ) ) ;
#77239=CARTESIAN_POINT ( 'NONE',  ( -21.09935167195790839, -4.734744157926700225, 11.49999999999999645 ) ) ;
#77240=ORIENTED_EDGE ( 'NONE', *, *, #27811, .T. ) ;
#77242=B_SPLINE_CURVE_WITH_KNOTS ( 'NONE', 3,
 ( #16963, #40311, #98323, #28830, #39302, #13590 ),
 .UNSPECIFIED., .F., .F.,
 ( 4, 2, 4 ),
 ( 2.661873927568507014E-05, 0.002253574034153483369, 0.004480529329031281843 ),
 .UNSPECIFIED. ) ;
#77245=CARTESIAN_POINT ( 'NONE',  ( -57.62287095715004881, -23.47596703998600276, 11.44779298504227683 ) ) ;
#77246=CARTESIAN_POINT ( 'NONE',  ( -16.90645664988545249, 14.66980924573920397, 11.49999999999998934 ) ) ;
#77247=EDGE_CURVE ( 'NONE', #37557, #24356, #26272, .T. ) ;
#77248=CARTESIAN_POINT ( 'NONE',  ( -47.54065078942323197, -24.35071581493542325, 9.817618358456030592 ) ) ;
#77251=CARTESIAN_POINT ( 'NONE',  ( -58.62287095715006302, -24.65952944569304250, 1.056160979905695463 ) ) ;
#77252=CARTESIAN_POINT ( 'NONE',  ( -49.54102043467515415, -24.35071581493542325, 9.817618358456035921 ) ) ;
#77253=EDGE_CURVE ( 'NONE', #6116, #5085, #16678, .T. ) ;
#77254=CARTESIAN_POINT ( 'NONE',  ( -62.62287095715004881, -29.50248528299804818, 1.056150453629034924 ) ) ;
#77256=CARTESIAN_POINT ( 'NONE',  ( -20.67734376658059858, -3.193854526364364954, -1.500000000000002220 ) ) ;
#77257=EDGE_CURVE ( 'NONE', #24519, #99951, #62366, .T. ) ;
#77259=CARTESIAN_POINT ( 'NONE',  ( -86.58837541417300088, -24.34968618360933945, 0.1864209137778916059 ) ) ;
#77261=CARTESIAN_POINT ( 'NONE',  ( -109.5571236054648523, -23.73791477778912551, 11.05961554403169878 ) ) ;
#77262=CARTESIAN_POINT ( 'NONE',  ( -17.67215177357914513, -11.65580189297658897, -1.500000000000002220 ) ) ;
#77263=ORIENTED_EDGE ( 'NONE', *, *, #76680, .F. ) ;
#77264=CARTESIAN_POINT ( 'NONE',  ( -50.52963312974734578, -24.83618233451449697, 1.606449574219540599 ) ) ;
#77265=FACE_OUTER_BOUND ( 'NONE', #89826, .T. ) ;
#77266=CARTESIAN_POINT ( 'NONE',  ( 14.98227958311676744, 15.82868232077399462, -1.500000000000002220 ) ) ;
#77267=PLANE ( 'NONE',  #51388 ) ;
#77269=CARTESIAN_POINT ( 'NONE',  ( -80.41333690452883332, -25.13350261022028675, 7.099562396224023963 ) ) ;
#77270=CARTESIAN_POINT ( 'NONE',  ( 3.267597511969735802, 21.59432767039258394, -1.500000000000002220 ) ) ;
#77271=CARTESIAN_POINT ( 'NONE',  ( -71.27229073968156570, -25.31639491978751622, 4.988759705255076504 ) ) ;
#77272=ORIENTED_EDGE ( 'NONE', *, *, #12776, .F. ) ;
#77278=VECTOR ( 'NONE', #60233, 1000.000000000000114 ) ;
#77280=EDGE_LOOP ( 'NONE', ( #72386, #41346, #59571, #72696 ) ) ;
#77281=CARTESIAN_POINT ( 'NONE',  ( -63.62287095715003460, -23.48783264082478084, -1.443836473390069042 ) ) ;
#77282=CARTESIAN_POINT ( 'NONE',  ( 20.83148622972472808, -3.941400823363257366, 11.49999999999998934 ) ) ;
#77283=CARTESIAN_POINT ( 'NONE',  ( -94.62287095715005592, -24.65952944569304606, 1.056160979905700348 ) ) ;
#77284=CARTESIAN_POINT ( 'NONE',  ( -79.02216967728209340, -25.27791743151245996, 6.505900957663475204 ) ) ;
#77285=CARTESIAN_POINT ( 'NONE',  ( -60.52287095715006160, -24.99156044556119838, 7.747789690856173195 ) ) ;
#77288=CARTESIAN_POINT ( 'NONE',  ( 11.20917403917954225, 15.81763734437701885, 11.49999999999998934 ) ) ;
#77289=CARTESIAN_POINT ( 'NONE',  ( -69.35003614255256821, -25.26766161569622682, 6.083062509053539735 ) ) ;
#77292=CARTESIAN_POINT ( 'NONE',  ( -9.780116039169133302, 16.78644576961053048, 11.49999999999999645 ) ) ;
#77293=LINE ( 'NONE', #7796, #56895 ) ;
#77295=CARTESIAN_POINT ( 'NONE',  ( -103.5228709571500758, -24.64965694238408034, 8.947790433994194714 ) ) ;
#77296=B_SPLINE_CURVE_WITH_KNOTS ( 'NONE', 3,
 ( #91913, #69593, #30518, #7683 ),
 .UNSPECIFIED., .F., .F.,
 ( 4, 4 ),
 ( 0.000000000000000000, 9.999999999998897304E-05 ),
 .UNSPECIFIED. ) ;
#77300=CARTESIAN_POINT ( 'NONE',  ( -91.62287095715004170, -23.47596703998600631, 11.44779298504227860 ) ) ;
#77301=EDGE_CURVE ( 'NONE', #87827, #29179, #54259, .T. ) ;
#77302=CARTESIAN_POINT ( 'NONE',  ( -93.51252845903317734, -24.15620529776628800, 10.23563542870659582 ) ) ;
#77303=CARTESIAN_POINT ( 'NONE',  ( -15.96901387740391343, -11.39031854172415947, 11.49999999999998934 ) ) ;
#77304=CARTESIAN_POINT ( 'NONE',  ( -117.6228709571500701, -24.66019654487199730, 8.947790411086121054 ) ) ;
#77306=CARTESIAN_POINT ( 'NONE',  ( 11.83326311654409935, 18.06170320929925310, -1.500000000000002220 ) ) ;
#77307=CARTESIAN_POINT ( 'NONE',  ( -120.5228709571500616, -24.99132157543167310, 2.256160258750667502 ) ) ;
#77309=B_SPLINE_CURVE_WITH_KNOTS ( 'NONE', 3,
 ( #41687, #96953, #35063, #9720, #80229, #72633, #48799, #89348, #3125, #26944, #33062, #34063, #65039, #73128, #42687, #25942 ),
 .UNSPECIFIED., .F., .F.,
 ( 4, 2, 2, 2, 2, 2, 2, 4 ),
 ( 2.602085213965210642E-18, 0.0002042144920037962993, 0.0004084289840075899965, 0.0006126434760113836937, 0.0008168579680151773909, 0.001225286952022764785, 0.001429501444026539184, 0.001633715936030313799 ),
 .UNSPECIFIED. ) ;
#77311=CARTESIAN_POINT ( 'NONE',  ( 7.103900956763240515, -21.94381868531750968, -1.500000000000002220 ) ) ;
#77314=PLANE ( 'NONE',  #35378 ) ;
#77316=CARTESIAN_POINT ( 'NONE',  ( -121.5550104420377409, -24.15620529776628800, 10.23563542870660115 ) ) ;
#77317=CARTESIAN_POINT ( 'NONE',  ( -104.5228709571500758, -23.47596703998600631, 11.44779298504228215 ) ) ;
#77318=CARTESIAN_POINT ( 'NONE',  ( -111.3477393431454487, -25.29823902580309891, 3.253010139271965251 ) ) ;
#77319=CARTESIAN_POINT ( 'NONE',  ( -129.6235277210520564, -24.51314013834316796, 0.6176544820404222813 ) ) ;
#77320=CARTESIAN_POINT ( 'NONE',  ( -99.32787325113280019, -25.31566036122295671, 4.639922477934026901 ) ) ;
#77321=CARTESIAN_POINT ( 'NONE',  ( 19.23997954701083657, -5.074110557352235595, 11.49999999999998934 ) ) ;
#77322=CARTESIAN_POINT ( 'NONE',  ( -41.52287095715005449, -23.48783264083359867, -1.443836473376375329 ) ) ;
#77323=CARTESIAN_POINT ( 'NONE',  ( -8.418173371947181849, -17.93405594323863284, -1.500000000000002220 ) ) ;
#77326=CARTESIAN_POINT ( 'NONE',  ( -108.5895376238167245, -24.64898659630368627, 1.056161002820390493 ) ) ;
#77327=FACE_OUTER_BOUND ( 'NONE', #91224, .T. ) ;
#77328=CARTESIAN_POINT ( 'NONE',  ( 20.74337371777590278, 0.4424840333690017724, 11.49999999999999645 ) ) ;
#77329=VECTOR ( 'NONE', #18534, 1000.000000000000114 ) ;
#77330=FACE_OUTER_BOUND ( 'NONE', #33871, .T. ) ;
#77332=CARTESIAN_POINT ( 'NONE',  ( -106.5895376238167387, -24.66019654487199730, 8.947790411086117501 ) ) ;
#77333=CARTESIAN_POINT ( 'NONE',  ( 22.70222466501550329, 0.2752559529566028229, 11.49999999999999645 ) ) ;
#77335=B_SPLINE_SURFACE_WITH_KNOTS ( 'NONE', 3, 3, ( 
 ( #93328, #15209, #22802, #14704 ),
 ( #30934, #76595, #69998, #1502 ),
 ( #45670, #485, #69506, #78590 ),
 ( #91830, #61405, #9100, #53788 ),
 ( #71012, #995, #99924, #92828 ),
 ( #46169, #61902, #23310, #62398 ),
 ( #7098, #38047, #16710, #69000 ) ),
 .UNSPECIFIED., .F., .F., .F.,
 ( 4, 3, 4 ),
 ( 4, 4 ),
 ( 0.7945040050992244751, 0.8970133687736505657, 0.9995227324480766562 ),
 ( 0.9197277128001624114, 0.9211650446997299291 ),
 .UNSPECIFIED. ) ;
#77336=DIRECTION ( 'NONE',  ( -3.773278334444166432E-23, 1.000000000000000000, 0.000000000000000000 ) ) ;
#77337=CARTESIAN_POINT ( 'NONE',  ( -106.6228709571500985, -24.33832256527048798, 0.1851278514138634534 ) ) ;
#77339=CARTESIAN_POINT ( 'NONE',  ( -16.67386609800740516, 11.36076560755915033, -1.500000000000002220 ) ) ;
#77341=CARTESIAN_POINT ( 'NONE',  ( -95.62287095715009855, -24.82558206586144323, 1.605769216559443935 ) ) ;
#77344=EDGE_LOOP ( 'NONE', ( #52552, #13875, #97464, #34198 ) ) ;
#77345=PLANE ( 'NONE',  #35507 ) ;
#77346=CARTESIAN_POINT ( 'NONE',  ( 12.20170062390598709, -19.39347807479101249, -1.500000000000002220 ) ) ;
#77347=CARTESIAN_POINT ( 'NONE',  ( -51.28182533633388829, -25.18439771871680577, 3.855515987445083503 ) ) ;
#77348=CARTESIAN_POINT ( 'NONE',  ( 17.85095790706337127, 12.24325521369631176, -1.500000000000002220 ) ) ;
#77349=CARTESIAN_POINT ( 'NONE',  ( -123.5905688118583470, -23.96119346886881019, -0.6495511937832022520 ) ) ;
#77350=CARTESIAN_POINT ( 'NONE',  ( -3.961239394588834895, 20.55660451852329018, 11.49999999999999645 ) ) ;
#77352=CARTESIAN_POINT ( 'NONE',  ( -68.94044447473358161, -25.31612700224413004, 6.138838773723374942 ) ) ;
#77353=CARTESIAN_POINT ( 'NONE',  ( -15.57331531552114612, -15.56871402003811333, -1.500000000000002220 ) ) ;
#77354=VECTOR ( 'NONE', #24717, 1000.000000000000114 ) ;
#77355=CARTESIAN_POINT ( 'NONE',  ( -127.4728709571500360, -25.21113200442379565, 5.000950862978372768 ) ) ;
#77356=CARTESIAN_POINT ( 'NONE',  ( -30.47287095715007155, -25.10123602413552035, 7.248486769786293138 ) ) ;
#77357=ORIENTED_EDGE ( 'NONE', *, *, #53700, .F. ) ;
#77360=ORIENTED_EDGE ( 'NONE', *, *, #29880, .T. ) ;
#77361=CARTESIAN_POINT ( 'NONE',  ( -72.50700632870835705, -24.15620529776627734, 10.23563542870660825 ) ) ;
#77364=VERTEX_POINT ( 'NONE', #38517 ) ;
#77365=ADVANCED_FACE ( 'NONE', ( #93804 ), #24297, .F. ) ;
#77366=CARTESIAN_POINT ( 'NONE',  ( -32.55620429048340014, -24.64898659630528854, 1.056161002820822592 ) ) ;
#77367=CARTESIAN_POINT ( 'NONE',  ( -74.52287095715007581, -29.50247984919015209, -1.443849546365055359 ) ) ;
#77369=CARTESIAN_POINT ( 'NONE',  ( 19.38413035786728145, -6.671778716439519030, -1.500000000000002220 ) ) ;
#77370=VERTEX_POINT ( 'NONE', #86194 ) ;
#77371=CARTESIAN_POINT ( 'NONE',  ( -71.62287095715005592, -23.73934037231757443, 11.05740245334328975 ) ) ;
#77372=CARTESIAN_POINT ( 'NONE',  ( -33.62287095715006302, -23.73934037231755667, 11.05740245334329508 ) ) ;
#77374=CARTESIAN_POINT ( 'NONE',  ( -19.83904684311861644, 10.14288308415042827, -1.500000000000002220 ) ) ;
#77376=CARTESIAN_POINT ( 'NONE',  ( -101.5228709571500758, -24.64898659630368627, 1.056161002820829697 ) ) ;
#77379=CARTESIAN_POINT ( 'NONE',  ( -39.52287095715006870, -24.66019654487198665, 8.947790411086131712 ) ) ;
#77381=CARTESIAN_POINT ( 'NONE',  ( -20.82185584224439978, -0.2524610531272265534, -1.500000000000002220 ) ) ;
#77382=EDGE_CURVE ( 'NONE', #2549, #3403, #27792, .T. ) ;
#77383=ORIENTED_EDGE ( 'NONE', *, *, #77992, .F. ) ;
#77384=CARTESIAN_POINT ( 'NONE',  ( -42.52287095715005449, -23.48786465467240347, 11.44779295918255180 ) ) ;
#77386=CARTESIAN_POINT ( 'NONE',  ( -50.85935151307011637, -25.12217849056909813, 7.039179954492152724 ) ) ;
#77387=CARTESIAN_POINT ( 'NONE',  ( 12.86141378215833342, 16.59024694808438127, -1.500000000000002220 ) ) ;
#77390=CARTESIAN_POINT ( 'NONE',  ( -55.62287095715004170, -24.14406661707768720, 10.28769366152059561 ) ) ;
#77392=B_SPLINE_CURVE_WITH_KNOTS ( 'NONE', 3,
 ( #51283, #18823, #43671, #34568, #82223, #56916 ),
 .UNSPECIFIED., .F., .F.,
 ( 4, 2, 4 ),
 ( 0.000000000000000000, 0.001380764517854766700, 0.002761529035709533401 ),
 .UNSPECIFIED. ) ;
#77394=CARTESIAN_POINT ( 'NONE',  ( -92.59430328945671818, -23.96169478059713498, 10.65365249895717881 ) ) ;
#77395=PLANE ( 'NONE',  #87015 ) ;
#77396=CARTESIAN_POINT ( 'NONE',  ( -14.87450875942801254, -16.50811611944624602, 11.49999999999999645 ) ) ;
#77398=EDGE_CURVE ( 'NONE', #4386, #91196, #83228, .T. ) ;
#77399=CARTESIAN_POINT ( 'NONE',  ( -37.62287095715005592, -23.48786465467240347, 11.44779295918255180 ) ) ;
#77400=EDGE_LOOP ( 'NONE', ( #97722, #18396, #18003, #55451 ) ) ;
#77401=CARTESIAN_POINT ( 'NONE',  ( -17.75566480456612695, 14.03706703302619374, -1.500000000000002220 ) ) ;
#77402=CARTESIAN_POINT ( 'NONE',  ( -111.5228709571500758, -23.96177878511310055, 10.65340807706329507 ) ) ;
#77404=ORIENTED_EDGE ( 'NONE', *, *, #92933, .T. ) ;
#77406=B_SPLINE_CURVE_WITH_KNOTS ( 'NONE', 3,
 ( #192, #62604, #31134, #54484, #15906, #77794 ),
 .UNSPECIFIED., .F., .F.,
 ( 4, 2, 4 ),
 ( 0.000000000000000000, 0.001380764517854763881, 0.002761529035709527763 ),
 .UNSPECIFIED. ) ;
#77407=CARTESIAN_POINT ( 'NONE',  ( -17.50950832565593984, 9.922426906265528146, -1.500000000000002220 ) ) ;
#77408=LINE ( 'NONE', #54109, #50602 ) ;
#77409=ORIENTED_EDGE ( 'NONE', *, *, #87332, .T. ) ;
#77411=CARTESIAN_POINT ( 'NONE',  ( -20.55042600948665310, 8.738301046694649798, -1.500000000000002220 ) ) ;
#77412=EDGE_CURVE ( 'NONE', #60463, #7274, #95803, .T. ) ;
#77414=ORIENTED_EDGE ( 'NONE', *, *, #32898, .T. ) ;
#77416=CARTESIAN_POINT ( 'NONE',  ( -94.58428862232342738, -24.66019654487199730, 8.947790411086121054 ) ) ;
#77418=CARTESIAN_POINT ( 'NONE',  ( -62.52287095715006160, -23.47593901973090169, -1.443836447538997092 ) ) ;
#77420=CARTESIAN_POINT ( 'NONE',  ( -30.64427850938830389, -23.47593901973090169, -1.443836447538998646 ) ) ;
#77421=CARTESIAN_POINT ( 'NONE',  ( 11.58774116221665729, 15.72987433093905096, 11.49999999999998934 ) ) ;
#77423=CARTESIAN_POINT ( 'NONE',  ( 10.13398631766115443, 18.95262098133242290, -1.500000000000002220 ) ) ;
#77424=CARTESIAN_POINT ( 'NONE',  ( -128.5559270644360481, -23.96119346886882084, -0.6495511937831803806 ) ) ;
#77425=CARTESIAN_POINT ( 'NONE',  ( -54.62287095715006302, -24.50321055353805377, 9.387540953477531147 ) ) ;
#77428=CARTESIAN_POINT ( 'NONE',  ( 22.56601425305882813, -3.627385684441148506, -1.500000000000002220 ) ) ;
#77432=DIRECTION ( 'NONE',  ( 3.773278334444166432E-23, -1.000000000000000000, 0.000000000000000000 ) ) ;
#77434=CARTESIAN_POINT ( 'NONE',  ( -9.072532997253766496, -17.89392090870456542, 11.49999999999999645 ) ) ;
#77437=AXIS2_PLACEMENT_3D ( 'NONE', #38617, #55362, #86293 ) ;
#77439=CARTESIAN_POINT ( 'NONE',  ( -39.58953762381673158, -23.47596703998600276, 11.44779298504227505 ) ) ;
#77442=CARTESIAN_POINT ( 'NONE',  ( -109.1326033789950145, -25.21121287918716902, 3.488800947434629762 ) ) ;
#77443=CARTESIAN_POINT ( 'NONE',  ( -21.53672441135761773, -2.854535511010750870, -1.500000000000002220 ) ) ;
#77444=PLANE ( 'NONE',  #35077 ) ;
#77445=CARTESIAN_POINT ( 'NONE',  ( -19.13235715846047214, 4.354950445902704637, -1.500000000000002220 ) ) ;
#77448=CARTESIAN_POINT ( 'NONE',  ( -109.8661607933284472, -25.27925885274750328, 5.216081408360091487 ) ) ;
#77450=B_SPLINE_CURVE_WITH_KNOTS ( 'NONE', 3,
 ( #82963, #84468, #54037, #62146, #14449, #77341, #14949, #93070 ),
 .UNSPECIFIED., .F., .F.,
 ( 4, 2, 2, 4 ),
 ( 0.000000000000000000, 0.002001098010032682350, 0.003001647015049025043, 0.004002196020065368169 ),
 .UNSPECIFIED. ) ;
#77451=PLANE ( 'NONE',  #41896 ) ;
#77452=CARTESIAN_POINT ( 'NONE',  ( -47.52287095715009713, -23.95044443724992789, 10.65354141964649415 ) ) ;
#77453=CARTESIAN_POINT ( 'NONE',  ( -19.39287000742378453, 6.875061630626206011, 11.49999999999999645 ) ) ;
#77454=CARTESIAN_POINT ( 'NONE',  ( -39.04496671189667723, -25.29399908399037145, 4.275509040138983252 ) ) ;
#77455=CARTESIAN_POINT ( 'NONE',  ( -47.62287095715004170, -24.65952944569304250, 1.056160979905693686 ) ) ;
#77458=CARTESIAN_POINT ( 'NONE',  ( -99.52764846858842418, -25.26387293761020914, 3.999772272046739907 ) ) ;
#77460=CARTESIAN_POINT ( 'NONE',  ( -74.52287095715007581, -24.50321055353805377, 9.387540953477508054 ) ) ;
#77461=CARTESIAN_POINT ( 'NONE',  ( -69.55620429048336462, -24.64965694238574656, 8.947790433994198267 ) ) ;
#77462=ADVANCED_FACE ( 'NONE', ( #79581 ), #8651, .T. ) ;
#77464=CARTESIAN_POINT ( 'NONE',  ( -32.52287095715006160, -23.47596703998600631, 11.44779298504229459 ) ) ;
#77467=CARTESIAN_POINT ( 'NONE',  ( -23.06710473063640165, 0.7821689226722955413, 11.49999999999999645 ) ) ;
#77468=CARTESIAN_POINT ( 'NONE',  ( 18.64237364862239943, 13.12531859369229359, 11.49999999999998934 ) ) ;
#77469=CARTESIAN_POINT ( 'NONE',  ( -74.55412977414610509, -23.96119346886879953, -0.6495511937832119109 ) ) ;
#77470=B_SPLINE_SURFACE_WITH_KNOTS ( 'NONE', 3, 3, ( 
 ( #94421, #54371, #85813, #41152 ),
 ( #24904, #23904, #94924, #93916 ),
 ( #15789, #32525, #70589, #79194 ),
 ( #64007, #62483, #2097, #1080 ),
 ( #61983, #31518, #55375, #86310 ),
 ( #2591, #9182, #16293, #71098 ),
 ( #39633, #24408, #39130, #40143 ) ),
 .UNSPECIFIED., .F., .F., .F.,
 ( 4, 3, 4 ),
 ( 4, 4 ),
 ( 0.0004766839783844487510, 0.1029713700210909688, 0.2054660560637974753 ),
 ( 0.3095727472661086721, 0.3107283081189128326 ),
 .UNSPECIFIED. ) ;
#77471=CARTESIAN_POINT ( 'NONE',  ( -67.52287095715003318, -23.73907113216989728, -1.053371485793251905 ) ) ;
#77472=CARTESIAN_POINT ( 'NONE',  ( -104.5228709571500758, -24.66019654487200441, 8.947790411086113949 ) ) ;
#77474=CARTESIAN_POINT ( 'NONE',  ( 20.43785579724129420, 9.289222182981756504, 11.49999999999999645 ) ) ;
#77477=CARTESIAN_POINT ( 'NONE',  ( -70.62287095715005592, -25.00182538069145011, 7.747789668545097541 ) ) ;
#77478=CARTESIAN_POINT ( 'NONE',  ( -17.33335002049248530, 13.43749923854009509, 11.49999999999998934 ) ) ;
#77479=FACE_OUTER_BOUND ( 'NONE', #76511, .T. ) ;
#77480=CARTESIAN_POINT ( 'NONE',  ( -87.59165135172374050, -24.15620529776628445, 10.23563542870660292 ) ) ;
#77481=FACE_OUTER_BOUND ( 'NONE', #77114, .T. ) ;
#77482=CARTESIAN_POINT ( 'NONE',  ( -129.6228709571500417, -29.50248528299804818, 1.056150453629047137 ) ) ;
#77484=ORIENTED_EDGE ( 'NONE', *, *, #51535, .F. ) ;
#77485=CARTESIAN_POINT ( 'NONE',  ( -20.46784169311667867, 0.4426517378232717737, -1.500000000000002220 ) ) ;
#77490=EDGE_CURVE ( 'NONE', #7016, #57758, #55395, .T. ) ;
#77491=CARTESIAN_POINT ( 'NONE',  ( -14.75821945985506645, 17.75411527500383002, 11.49999999999998934 ) ) ;
#77492=DIRECTION ( 'NONE',  ( 3.773278334444166432E-23, -1.000000000000000000, 0.000000000000000000 ) ) ;
#77493=CARTESIAN_POINT ( 'NONE',  ( 9.679018533540549640, -17.85022214266596308, -1.500000000000002220 ) ) ;
#77496=AXIS2_PLACEMENT_3D ( 'NONE', #68859, #29794, #84074 ) ;
#77497=CARTESIAN_POINT ( 'NONE',  ( -72.52287095715006160, -24.50216790748204332, 0.6166512839542518387 ) ) ;
#77499=CARTESIAN_POINT ( 'NONE',  ( -99.63766830052645673, -23.48786465467241413, 11.44779295918254292 ) ) ;
#77500=CARTESIAN_POINT ( 'NONE',  ( -15.45034113870702441, -14.97902827799142500, 11.49999999999999645 ) ) ;
#77502=CARTESIAN_POINT ( 'NONE',  ( -75.58062029086705991, -24.92564183028979130, 1.928384488918256645 ) ) ;
#77503=CARTESIAN_POINT ( 'NONE',  ( -61.55369053405362934, -23.96169478059712787, 10.65365249895718591 ) ) ;
#77504=VERTEX_POINT ( 'NONE', #59754 ) ;
#77505=CARTESIAN_POINT ( 'NONE',  ( 17.59156710592704442, 10.99281682905060897, -1.500000000000002220 ) ) ;
#77507=ORIENTED_EDGE ( 'NONE', *, *, #25163, .F. ) ;
#77509=VERTEX_POINT ( 'NONE', #98283 ) ;
#77512=CARTESIAN_POINT ( 'NONE',  ( -48.52287095715004028, -24.34917612407046050, 0.1852690917481008004 ) ) ;
#77513=ORIENTED_EDGE ( 'NONE', *, *, #55997, .F. ) ;
#77514=ORIENTED_EDGE ( 'NONE', *, *, #87170, .T. ) ;
#77517=CARTESIAN_POINT ( 'NONE',  ( -42.61655362215102372, -23.48786465467240347, 11.44779295918255535 ) ) ;
#77518=CARTESIAN_POINT ( 'NONE',  ( -65.54247407030995021, -24.52300882791528736, 0.6510814631126250474 ) ) ;
#77519=CARTESIAN_POINT ( 'NONE',  ( 19.49364837986538745, 10.19379059548657551, 11.49999999999999645 ) ) ;
#77522=CARTESIAN_POINT ( 'NONE',  ( -8.633696204196466439, -20.85254729778420923, -1.500000000000002220 ) ) ;
#77523=CARTESIAN_POINT ( 'NONE',  ( 12.56776941831905070, -16.83212535568997126, -1.500000000000002220 ) ) ;
#77525=CARTESIAN_POINT ( 'NONE',  ( -127.5228709571500616, -29.50250243563736774, 8.947779886222132717 ) ) ;
#77526=EDGE_LOOP ( 'NONE', ( #18755, #94913, #19619, #82279 ) ) ;
#77527=ADVANCED_FACE ( 'NONE', ( #13053 ), #28790, .T. ) ;
#77530=FACE_OUTER_BOUND ( 'NONE', #5288, .T. ) ;
#77531=CARTESIAN_POINT ( 'NONE',  ( -20.54356019850136050, 6.435454313062578535, -1.500000000000002220 ) ) ;
#77534=CARTESIAN_POINT ( 'NONE',  ( 1.812468502196824760, -21.08352789287561180, -1.500000000000002220 ) ) ;
#77535=CARTESIAN_POINT ( 'NONE',  ( -126.6228709571501696, -24.51283580621365132, 0.6167428607019908027 ) ) ;
#77536=CARTESIAN_POINT ( 'NONE',  ( -60.72641359848758214, -25.29489609436098263, 6.057563354383567855 ) ) ;
#77537=CARTESIAN_POINT ( 'NONE',  ( -121.5198938983199923, -24.15543982623907127, -0.2315651400026573492 ) ) ;
#77539=CARTESIAN_POINT ( 'NONE',  ( -127.5228709571500332, -23.73934037231757443, 11.05740245334327199 ) ) ;
#77540=CARTESIAN_POINT ( 'NONE',  ( -20.56814720681451902, 8.302189128749821734, -1.500000000000002220 ) ) ;
#77541=CARTESIAN_POINT ( 'NONE',  ( -71.58416595370849222, -24.51314013834315730, 0.6176544820404130665 ) ) ;
#77544=LINE ( 'NONE', #70454, #70317 ) ;
#77545=CARTESIAN_POINT ( 'NONE',  ( -126.6242557217197628, -24.15543982623907482, -0.2315651400026573492 ) ) ;
#77547=FACE_OUTER_BOUND ( 'NONE', #40476, .T. ) ;
#77548=CARTESIAN_POINT ( 'NONE',  ( 19.04819733361787470, -3.913502273677552878, -1.500000000000002220 ) ) ;
#77549=CARTESIAN_POINT ( 'NONE',  ( -0.4629837013611828866, -21.40787533109759977, -1.500000000000002220 ) ) ;
#77550=CARTESIAN_POINT ( 'NONE',  ( -62.59277767315021634, -24.15543982623907482, -0.2315651400026649265 ) ) ;
#77553=CARTESIAN_POINT ( 'NONE',  ( -38.58953762381673158, -24.65952944569304250, 1.056160979905691022 ) ) ;
#77554=CARTESIAN_POINT ( 'NONE',  ( -2.919094682108430483, 22.50186656173435296, -1.500000000000002220 ) ) ;
#77555=B_SPLINE_SURFACE_WITH_KNOTS ( 'NONE', 3, 3, ( 
 ( #81573, #88191, #49636, #89187 ),
 ( #88689, #63875, #80566, #11061 ),
 ( #19159, #41020, #12047, #65873 ),
 ( #42027, #43017, #73960, #27288 ),
 ( #72970, #96792, #34399, #65376 ),
 ( #96297, #32904, #57749, #18172 ),
 ( #95298, #17670, #58243, #94790 ) ),
 .UNSPECIFIED., .F., .F., .F.,
 ( 4, 3, 4 ),
 ( 4, 4 ),
 ( 0.0004766839783814693634, 0.1029713700210893174, 0.2054660560637971700 ),
 ( 0.5296287257475410515, 0.5308858200244782610 ),
 .UNSPECIFIED. ) ;
#77556=CARTESIAN_POINT ( 'NONE',  ( -63.52287095715006160, -23.48786465467241058, 11.44779295918254824 ) ) ;
#77557=PLANE ( 'NONE',  #86482 ) ;
#77558=CARTESIAN_POINT ( 'NONE',  ( 8.615496892348360802, 17.92367856960711947, 11.49999999999999645 ) ) ;
#77559=CARTESIAN_POINT ( 'NONE',  ( -123.5215655060820410, -23.73791477778912196, 11.05961554403169878 ) ) ;
#77561=CARTESIAN_POINT ( 'NONE',  ( -61.64687923781919920, -25.20074463982482982, 3.409327697717700278 ) ) ;
#77562=B_SPLINE_CURVE_WITH_KNOTS ( 'NONE', 3,
 ( #96128, #27617, #82878, #82387 ),
 .UNSPECIFIED., .F., .F.,
 ( 4, 4 ),
 ( 0.000000000000000000, 9.999999999998897304E-05 ),
 .UNSPECIFIED. ) ;
#77563=VERTEX_POINT ( 'NONE', #98788 ) ;
#77566=CARTESIAN_POINT ( 'NONE',  ( -115.5895376238167387, -25.00158670708909625, 2.256160236439167299 ) ) ;
#77567=CARTESIAN_POINT ( 'NONE',  ( 4.348677445931066643, 21.19853102677161871, 11.49999999999998934 ) ) ;
#77568=CARTESIAN_POINT ( 'NONE',  ( -124.5228709571500616, -24.64898659630368627, 1.056161002820833028 ) ) ;
#77570=CARTESIAN_POINT ( 'NONE',  ( -18.32239908988104204, -6.426282940459683068, -1.500000000000002220 ) ) ;
#77571=CARTESIAN_POINT ( 'NONE',  ( -55.47780762501948715, -25.00182538069146787, 7.747789668545041586 ) ) ;
#77572=CARTESIAN_POINT ( 'NONE',  ( -3.387584560642538101, 19.54024307811383210, -1.500000000000002220 ) ) ;
#77573=VERTEX_POINT ( 'NONE', #91674 ) ;
#77574=CARTESIAN_POINT ( 'NONE',  ( -16.54958403137900191, 11.88860064210666856, 11.49999999999999645 ) ) ;
#77575=CARTESIAN_POINT ( 'NONE',  ( -80.63292597169439091, -24.52300882791530157, 0.6510814631126378149 ) ) ;
#77577=EDGE_CURVE ( 'NONE', #14489, #93507, #14208, .T. ) ;
#77579=CARTESIAN_POINT ( 'NONE',  ( -78.95130178854248015, -25.24824198256244401, 6.186328973465725412 ) ) ;
#77581=CARTESIAN_POINT ( 'NONE',  ( -96.62287095715007013, -23.72773821059535848, 11.05748984161097503 ) ) ;
#77584=CARTESIAN_POINT ( 'NONE',  ( -127.6228709571500559, -23.72773821059535848, 11.05748984161097503 ) ) ;
#77585=CARTESIAN_POINT ( 'NONE',  ( 19.44710440357065551, 5.058846670610233076, -1.500000000000002220 ) ) ;
#77588=EDGE_CURVE ( 'NONE', #96640, #12730, #78369, .T. ) ;
#77589=CARTESIAN_POINT ( 'NONE',  ( -129.5895376238167387, -23.47593901973091235, -1.443836447538995760 ) ) ;
#77592=CARTESIAN_POINT ( 'NONE',  ( -22.79553223295561892, 1.966428799096173075, 11.49999999999999645 ) ) ;
#77593=CARTESIAN_POINT ( 'NONE',  ( -14.94938274637043207, -17.11189489004485864, -1.500000000000002220 ) ) ;
#77594=ORIENTED_EDGE ( 'NONE', *, *, #92901, .T. ) ;
#77595=CARTESIAN_POINT ( 'NONE',  ( -81.11505102485448049, -25.26845562246343846, 3.692626550805397478 ) ) ;
#77596=CARTESIAN_POINT ( 'NONE',  ( -28.52287095715005805, -24.49893655963190042, 1.056161680022248195 ) ) ;
#77597=CARTESIAN_POINT ( 'NONE',  ( -39.86131625157400293, -25.21721466608290640, 3.456295588647256611 ) ) ;
#77599=CARTESIAN_POINT ( 'NONE',  ( -30.57287095715005165, -24.99054282775755098, 7.805183119964042682 ) ) ;
#77600=CARTESIAN_POINT ( 'NONE',  ( -55.62287095715004881, -25.00158670708909625, 2.256160236439165967 ) ) ;
#77601=CLOSED_SHELL ( 'NONE', ( #48213, #23166, #28225, #30506, #57841, #86485, #56552, #7050, #81895, #80534, #30560, #78275, #50275, #39693, #43596, #1947, #71652, #61465, #44224, #42356, #51152, #14603, #37216, #48891, #15198, #23887, #3578, #67441, #85732, #23994, #95151, #41698, #16830, #1349, #3889, #95592, #100322, #42217, #73257, #17071, #29551, #69597, #19413, #46796, #44038, #3639, #16368, #46629, #17067, #40058, #89931, #10051, #90548, #76122, #69950, #15419, #27320, #11841, #12768, #61145, #10492, #53822, #33396, #70475, #89133, #62602, #84945, #50046, #18280, #25188, #7037, #12462, #4859, #33487, #9936, #20981, #18832, #57045, #66556, #95458, #56079, #79482, #65327, #37457, #60141, #2136, #40506, #59348, #12382, #67326, #92332, #70729, #12656, #18157, #11686, #86361, #36259, #40994, #84309, #83440, #82094, #10713, #55653, #35499, #35383, #21685, #1899, #98168, #88852, #91845, #32536, #16615, #36166, #99792, #58499, #61138, #82216, #50656, #56429, #78180, #85101, #39359, #58043, #88440, #64690, #8198, #74981, #85064, #51539, #57422, #92037, #23046, #88275, #31544, #17329, #87379, #99480, #70180, #99170, #96043, #43881, #61466, #50364, #32365, #98657, #86424, #78266, #90208, #96736, #61638, #52243, #42388, #19591, #65384, #18283, #36068, #94903, #24076, #48711, #4254, #4918, #76358, #67444, #45326, #35134, #62852, #29297, #11690, #14821, #66457, #15539, #99695, #50475, #38196, #84347, #85169, #32811, #43151, #43024, #70862, #18273, #30902, #59660, #72428, #42341, #41297, #77527, #53315, #50919, #11282, #35691, #11521, #92030, #22967, #25327, #43370, #26802, #74400, #98357, #86611, #31816, #93068, #18290, #66587, #55858, #38574, #43517, #54823, #7404, #64943, #74406, #99261, #20105, #76821, #60176, #72501, #90650, #75121, #22835, #61316, #9712, #88164, #1153, #79602, #25185, #25388, #3291, #49287, #41970, #49469, #34444, #16477, #57489, #90122, #21728, #11969, #44047, #80568, #42149, #72130, #98806, #55977, #3214, #57884, #26035, #10837, #58994, #90339, #35358, #36277, #30046, #45237, #29380, #39356, #83196, #76850, #97778, #6347, #75185, #16188, #12459, #22362, #44240, #14614, #60905, #59431, #92409, #97555, #13703, #19161, #91692, #79726, #81200, #62861, #86538, #95153, #52183, #11692, #58402, #73952, #55664, #92152, #87058, #63015, #52636, #7349, #100372, #90035, #46395, #27159, #70070, #53711, #66427, #57533, #21677, #92850, #67119, #37162, #4024, #20410, #72061, #78988, #11764, #56448, #14712, #36338, #70184, #10254, #62907, #99919, #45537, #81103, #90454, #61701, #36826, #73375, #14335, #61463, #86666, #68176, #18072, #29186, #26118, #90129, #93630, #29061, #83455, #36720, #81520, #79992, #33227, #85801, #16209, #3192, #52019, #70039, #4128, #20718, #53919, #68264, #38351, #87500, #85536, #47255, #81979, #5084, #53, #58533, #13212, #36996, #45366, #93662, #50359, #90215, #43034, #49702, #93322, #93928, #68789, #67514, #91161, #30761, #9122, #65530, #59305, #5028, #8296, #94282, #70990, #60129, #79909, #41067, #46982, #85040, #75874, #68785, #69827, #32227, #38092, #17521, #52660, #4794, #80014, #36520, #6953, #5584, #61469, #19280, #87705, #70093, #80423, #4596, #65449, #47164, #51075, #80341, #43836, #7798, #86205, #14153, #47875, #40982, #30521, #27443, #82952, #46109, #79036, #61990, #46687, #32800, #24795, #31588, #24792, #28251, #14724, #37120, #860, #77049, #40845, #95321, #96222, #84217, #74548, #7199, #22927, #68335, #92046, #3538, #71306, #6145, #87287, #34652, #26683, #86570, #60571, #56221, #80612, #65114, #10366, #35516, #89520, #63027, #29269, #33164, #25535, #13537, #69119, #94569, #55596, #55392, #10642, #71425, #73438, #2719, #24244, #54135, #600, #62642, #7391, #17833, #34795, #90664, #93352, #54255, #46171, #94349, #16310, #47951, #31963, #19082, #9321, #34010, #22918, #38561, #37287, #54708, #69256, #58969, #95071, #61384, #20109, #76495, #551, #11398, #61951, #2975, #50232, #42639, #46479, #72624, #60742, #32598, #32254, #25784, #32468, #19020, #62147, #58778, #8629, #50377, #57160, #32244, #96136, #40030, #66709, #66703, #35466, #91283, #12101, #81380, #67606, #38003, #41524, #94332, #86710, #84418, #20217, #56346, #71550, #80234, #78413, #18405, #54205, #64558, #75996, #28632, #65765, #39790, #85770, #43944, #63801, #80582, #54985, #42238, #77, #57001, #1004, #7720, #66956, #37410, #97685, #94687, #39072, #75597, #47634, #15660, #69145, #44539, #82204, #62141, #53244, #24138, #13778, #81965, #15053, #90160, #42849, #67645, #34511, #60502, #24171, #65513, #16234, #73099, #90412, #6297, #41372, #81596, #55285, #94946, #38996, #82084, #70029, #39154, #62764, #72745, #77365, #82247, #60593, #22962, #11844, #33165, #87457, #19775, #69310, #45207, #7156, #33380, #64826, #4829, #83107, #13204, #31020, #7614, #47505, #99925, #21788, #7147, #12594, #66121, #46023, #28698, #21816, #33424, #6265, #26304, #78263, #24220, #55223, #35836, #69710, #68700, #3786, #76118, #61644, #67568, #61139, #7611, #18468, #47433, #68215, #966, #85042, #87132, #87695, #43599, #29680, #38205, #13898, #61253, #50388, #54035, #78913, #96694, #4013, #100138, #76854, #86784, #45999, #7212, #48121, #85039, #97450, #1235, #63730, #48078, #95648, #73249, #26687, #100370, #89332, #18036, #50595, #19219, #37151, #23683, #40959, #85289, #67432, #58629, #62546, #83445, #11566, #96158, #29845, #85793, #46123, #60617, #18162, #73831, #21046, #62627, #98453, #66271, #22409, #51855, #5689, #732, #25273, #2842, #12977, #66973, #63368, #17092, #29378, #46626, #79253, #74850, #47020, #53328, #95438, #62391, #1496, #70777, #6962, #36141, #86338, #19855, #70151, #36766, #10512, #64996, #87820, #81207, #68808, #33805, #15623, #27135, #5662, #15566, #22386, #71726, #60628, #33842, #70716, #9022, #31856, #44849, #28138, #31407, #66781, #5268, #80939, #2129, #65630, #8679, #89977, #75026, #2382, #86184, #27195, #28485, #42683, #33399, #69618, #59748, #27036, #45877, #26931, #99306, #2999, #41893, #39858, #32190, #2623, #63178, #68623, #99915, #74968, #88749, #42233, #87600, #39853, #13774, #41250, #24713, #98345, #81016, #71851, #59690, #23765, #33874, #99363, #64117, #65868, #19895, #66884, #42275, #3173, #38080, #79681, #90349, #76285, #67314, #96215, #4968, #38331, #55959, #68499, #59563, #13669, #7277, #52470, #40180, #61595, #39108, #34435, #45001, #73503, #22613, #55105, #14082, #4207, #25412, #59555, #26926, #30327, #41013, #84595, #5967, #6131, #76450, #67115, #82812, #57679, #94166, #93166, #19758, #7727, #65335, #71610, #99836, #53809, #33505, #63347, #3734, #2313, #62138, #81057, #99247, #36135, #99203, #76191, #91068, #78406, #47767, #55881, #71, #25459, #41078, #74934, #39043, #98904, #96890, #94800, #8192, #37196, #10718, #99482, #36400, #97781, #13667, #81640, #41787, #74444, #87489, #5327, #77866, #93294, #3735, #64289, #39244, #67323, #8449, #42472, #69884, #93505, #43533, #5470, #97094, #66462, #39868, #26771, #98949, #80021, #48298, #51620, #81968, #74185, #96561, #77834, #53306, #57792, #98576, #65193, #66642, #43620, #97156, #69113, #40981, #11780, #31337, #96290, #39487, #29791, #14146, #77819, #79088, #51334, #161, #76751, #10836, #85216, #11642, #16794, #9885, #40381, #91575, #25937, #5116, #21295, #15505, #30125, #34876, #50840, #19910, #97533, #8600, #42722, #75116, #41662, #96008, #40737, #14965, #66403, #47179, #57920, #75876, #82697, #40512, #95200, #80126, #62962, #85324, #2139, #46402, #81003, #85859, #37084, #25218, #26178, #24118, #58405, #46607, #45671, #23506, #64176, #46861, #611, #99587, #90900, #79340, #2521, #17021, #86798, #55963, #70612, #42169, #3568, #40290, #56726, #25348, #58223, #39128, #37980, #36065, #50769, #61484, #69517, #18586, #3854, #30784, #52716, #70299, #4922, #47290, #32472, #95576, #1478, #96178, #61354, #36714, #51097, #25538, #96394, #97530, #5448, #25848, #49607, #50476, #50922, #70279, #11173, #83311, #36959, #92254, #52775, #61067, #59299, #69586, #61386, #81378, #87580, #5667, #46827, #17018, #95454, #72419, #3350, #91730, #89670, #11083, #45342, #63796, #87295, #89852, #56585, #54017, #29143, #67565, #15290, #56104, #84585, #12327, #10156, #74057, #78830, #1120, #29534, #26688, #29721, #84251, #36189, #79587, #15800, #96862, #19833, #12379, #64124, #34793, #91606, #39727, #96402, #53333, #2004, #75520, #95273, #14355, #90594, #76948, #28726, #42838, #54327, #13151, #57715, #85278, #29540, #58336, #86309, #82533, #91444, #24789, #6539, #90722, #11304, #57813, #15047, #38313, #81191, #72824, #14363, #68610, #852, #6700, #5038, #36025, #20157, #98227, #27045, #81306, #93742, #6159, #82560, #78840, #32418, #70881, #39224, #41456, #42909, #35395, #52404, #30768, #54288, #57741, #94046, #30079, #33680, #83669, #57744, #90507, #49364, #1570, #47282, #98672, #25144, #97980, #46566, #89429, #35873, #92360, #33332, #58292, #43707, #96405, #1732, #86986, #4239, #91137, #72179, #68442, #31203, #69383, #23404, #16559, #80129, #11168, #9858, #99294, #47704, #23493, #48779, #39063, #29945, #80732, #77462, #65261, #58606, #18902, #47559, #4219, #7267, #25277, #58039, #87689, #53909, #51040, #18709, #16202, #31542, #98339, #17397, #88646, #21153, #97998, #96091, #74511, #14928, #35472, #8122, #89207, #69387, #76897, #98602, #66021, #36296, #89791, #69705, #71108, #73871, #55791, #35084, #52067, #54947, #75073, #61714 ) ) ;
#77604=CARTESIAN_POINT ( 'NONE',  ( 2.554409723529738052, 20.22502395925995700, -1.500000000000002220 ) ) ;
#77605=ORIENTED_EDGE ( 'NONE', *, *, #16471, .T. ) ;
#77607=CARTESIAN_POINT ( 'NONE',  ( -16.20615075098634961, 16.30094363606528418, 11.49999999999998934 ) ) ;
#77608=CARTESIAN_POINT ( 'NONE',  ( -103.5562042904834072, -23.48783264082478794, -1.443836473390061492 ) ) ;
#77610=DIRECTION ( 'NONE',  ( -1.000000000000000000, -3.773278334444166432E-23, -8.201307841325785021E-29 ) ) ;
#77612=EDGE_CURVE ( 'NONE', #5568, #39979, #51796, .T. ) ;
#77613=CARTESIAN_POINT ( 'NONE',  ( -51.56793223790934633, -23.48786465467241058, 11.44779295918254824 ) ) ;
#77614=CARTESIAN_POINT ( 'NONE',  ( 16.11712757473013014, 13.99349609535929773, 11.49999999999999645 ) ) ;
#77615=VERTEX_POINT ( 'NONE', #6947 ) ;
#77617=CARTESIAN_POINT ( 'NONE',  ( 13.49617185221842952, 17.62045156095830123, 11.49999999999998934 ) ) ;
#77618=CARTESIAN_POINT ( 'NONE',  ( 14.23986175545555355, -14.96101607593195304, -1.500000000000002220 ) ) ;
#77620=ORIENTED_EDGE ( 'NONE', *, *, #95586, .F. ) ;
#77621=ORIENTED_EDGE ( 'NONE', *, *, #55709, .F. ) ;
#77622=CARTESIAN_POINT ( 'NONE',  ( -109.8650282762807393, -25.31627469272110531, 5.784627927385296964 ) ) ;
#77623=CARTESIAN_POINT ( 'NONE',  ( -95.63007649029256640, -24.52399227489127398, 9.353111116836521077 ) ) ;
#77625=VECTOR ( 'NONE', #91091, 1000.000000000000227 ) ;
#77626=CARTESIAN_POINT ( 'NONE',  ( -91.56188552897437205, -23.48783264082477018, -1.443836473390090802 ) ) ;
#77627=VECTOR ( 'NONE', #48424, 1000.000000000000227 ) ;
#77629=CARTESIAN_POINT ( 'NONE',  ( -58.63231504519726656, -24.35071581493543036, 9.817618358456028815 ) ) ;
#77630=CARTESIAN_POINT ( 'NONE',  ( -44.52287095715006870, -24.33832256527048088, 0.1851278514138559594 ) ) ;
#77631=CARTESIAN_POINT ( 'NONE',  ( -2.100290975465340271, -20.70549805216813510, -1.500000000000002220 ) ) ;
#77632=CARTESIAN_POINT ( 'NONE',  ( -17.45706314325883213, 13.02611496694466275, 11.49999999999999645 ) ) ;
#77633=EDGE_CURVE ( 'NONE', #57780, #94513, #35971, .T. ) ;
#77634=DIRECTION ( 'NONE',  ( 1.000000000000000000, 3.773278334444166432E-23, 8.201307841325785021E-29 ) ) ;
#77636=CARTESIAN_POINT ( 'NONE',  ( 8.471766090126642723, -20.80389698432254519, -1.500000000000002220 ) ) ;
#77637=VECTOR ( 'NONE', #76258, 1000.000000000000114 ) ;
#77638=EDGE_CURVE ( 'NONE', #18516, #4528, #69942, .T. ) ;
#77639=CARTESIAN_POINT ( 'NONE',  ( -44.58953762381671737, -24.64898659630528854, 1.056161002820819927 ) ) ;
#77640=CARTESIAN_POINT ( 'NONE',  ( -50.52287095715006160, -23.85229601348995843, 10.88205029486208453 ) ) ;
#77642=AXIS2_PLACEMENT_3D ( 'NONE', #76604, #22813, #82731 ) ;
#77643=ORIENTED_EDGE ( 'NONE', *, *, #85452, .F. ) ;
#77646=EDGE_CURVE ( 'NONE', #39432, #81122, #54140, .T. ) ;
#77647=ORIENTED_EDGE ( 'NONE', *, *, #30509, .F. ) ;
#77648=CARTESIAN_POINT ( 'NONE',  ( -6.196366259867160942, 20.41550611124569059, -1.500000000000002220 ) ) ;
#77649=ORIENTED_EDGE ( 'NONE', *, *, #82823, .T. ) ;
#77650=CARTESIAN_POINT ( 'NONE',  ( -14.29351441246084065, -15.47709782942846424, 11.49999999999998934 ) ) ;
#77652=CARTESIAN_POINT ( 'NONE',  ( -6.132916590032589710, 18.96384228413732842, -1.500000000000002220 ) ) ;
#77653=CARTESIAN_POINT ( 'NONE',  ( -114.5895376238167245, -23.48786465467241769, 11.44779295918253936 ) ) ;
#77654=CARTESIAN_POINT ( 'NONE',  ( -49.54749379695226708, -25.08548750068662869, 7.358461225295097385 ) ) ;
#77655=CARTESIAN_POINT ( 'NONE',  ( -17.28599015371049674, 13.57978550619682956, -1.500000000000002220 ) ) ;
#77656=CARTESIAN_POINT ( 'NONE',  ( -76.55620429048340725, -24.65952944569304606, 1.056160979905700126 ) ) ;
#77658=DIRECTION ( 'NONE',  ( 0.000000000000000000, 0.9999999999976377785, 2.173523156925979975E-06 ) ) ;
#77659=CARTESIAN_POINT ( 'NONE',  ( -54.55620429048340014, -23.47596703998600276, 11.44779298504227505 ) ) ;
#77660=CARTESIAN_POINT ( 'NONE',  ( 20.84756458399398937, 0.1950554047328266483, 11.49999999999999645 ) ) ;
#77662=CARTESIAN_POINT ( 'NONE',  ( -122.5228709571500616, -29.50248528299804818, 1.056150453629045360 ) ) ;
#77663=CARTESIAN_POINT ( 'NONE',  ( -20.38992493328631284, -24.51868705080920563, 5.002395802403317049 ) ) ;
#77664=CARTESIAN_POINT ( 'NONE',  ( 17.02398533174402218, 12.79255474601471043, -1.500000000000002220 ) ) ;
#77665=CARTESIAN_POINT ( 'NONE',  ( -98.56083136990402238, -23.48786465467241769, 11.44779295918254469 ) ) ;
#77669=CARTESIAN_POINT ( 'NONE',  ( -1.726696889551340153, 22.42386595106472669, -1.500000000000002220 ) ) ;
#77671=EDGE_LOOP ( 'NONE', ( #50300, #57496, #46327, #53113 ) ) ;
#77673=CARTESIAN_POINT ( 'NONE',  ( -5.193715590271882121, 18.98282465337476665, 11.49999999999999645 ) ) ;
#77674=CARTESIAN_POINT ( 'NONE',  ( -68.62287095715002749, -23.94994826722515668, -0.6494450866351699769 ) ) ;
#77676=ORIENTED_EDGE ( 'NONE', *, *, #14474, .F. ) ;
#77678=CARTESIAN_POINT ( 'NONE',  ( -84.62287095715005592, -23.47593901973091235, -1.443836447539004642 ) ) ;
#77679=CARTESIAN_POINT ( 'NONE',  ( -88.87267940187761894, -25.12049752546737835, 2.832404795212227100 ) ) ;
#77680=CARTESIAN_POINT ( 'NONE',  ( -70.35718658181241381, -25.12219144531794157, 7.100646793647915622 ) ) ;
#77681=CARTESIAN_POINT ( 'NONE',  ( 10.86211995951333620, 16.47970581058804740, -1.500000000000002220 ) ) ;
#77686=ORIENTED_EDGE ( 'NONE', *, *, #97466, .F. ) ;
#77687=DIRECTION ( 'NONE',  ( 0.000000000000000000, 0.9999999999976377785, 2.173523156925979128E-06 ) ) ;
#77688=CARTESIAN_POINT ( 'NONE',  ( -67.62287095715005592, -23.48783264082478794, -1.443836473390067265 ) ) ;
#77690=CARTESIAN_POINT ( 'NONE',  ( -99.00488046896290939, -25.26638346776037736, 6.667019968706677346 ) ) ;
#77692=EDGE_CURVE ( 'NONE', #48998, #6520, #72731, .T. ) ;
#77693=PLANE ( 'NONE',  #95954 ) ;
#77694=EDGE_CURVE ( 'NONE', #75484, #21744, #93171, .T. ) ;
#77695=CARTESIAN_POINT ( 'NONE',  ( -30.30597055170165888, -23.44955593248640824, -1.443836447538997314 ) ) ;
#77696=CARTESIAN_POINT ( 'NONE',  ( -18.86779840422491716, -6.689013621249945807, -1.500000000000002220 ) ) ;
#77698=CARTESIAN_POINT ( 'NONE',  ( -99.21726371882367346, -25.27533020790543361, 3.564824879032668203 ) ) ;
#77702=EDGE_CURVE ( 'NONE', #65722, #73093, #8113, .T. ) ;
#77703=VECTOR ( 'NONE', #30575, 1000.000000000000114 ) ;
#77704=CARTESIAN_POINT ( 'NONE',  ( -79.62649533826925108, -24.51419770103157347, 9.386484678747176957 ) ) ;
#77705=CARTESIAN_POINT ( 'NONE',  ( -109.5745106736623029, -25.29012798628001946, 3.630693211477457716 ) ) ;
#77706=CARTESIAN_POINT ( 'NONE',  ( -34.62287095715005592, -23.48786465467240347, 11.44779295918255535 ) ) ;
#77707=CARTESIAN_POINT ( 'NONE',  ( -92.52287095715006160, -23.48783264083452593, -1.443836473374927820 ) ) ;
#77709=CARTESIAN_POINT ( 'NONE',  ( -116.6623340026854692, -25.38352273315421925, 4.245316684715564115 ) ) ;
#77710=CARTESIAN_POINT ( 'NONE',  ( -54.62287095715005592, -24.65952944569304606, 1.056160979905694131 ) ) ;
#77711=AXIS2_PLACEMENT_3D ( 'NONE', #39716, #17893, #1169 ) ;
#77713=EDGE_CURVE ( 'NONE', #94877, #25496, #18432, .T. ) ;
#77716=CARTESIAN_POINT ( 'NONE',  ( 17.44645523915803764, -10.38078700900905993, -1.500000000000002220 ) ) ;
#77718=CARTESIAN_POINT ( 'NONE',  ( -39.56136241089613748, -25.30385213834873781, 5.536731319770037629 ) ) ;
#77719=ORIENTED_EDGE ( 'NONE', *, *, #78191, .T. ) ;
#77720=CARTESIAN_POINT ( 'NONE',  ( -83.55620429048339304, -23.48786465467241058, 11.44779295918254469 ) ) ;
#77721=CARTESIAN_POINT ( 'NONE',  ( 1.236116150138429903, -20.07036509671028668, -1.500000000000002220 ) ) ;
#77722=CARTESIAN_POINT ( 'NONE',  ( 17.90021246794804810, -11.17811638239879279, 11.49999999999999645 ) ) ;
#77723=CARTESIAN_POINT ( 'NONE',  ( -21.04927197579530329, -6.814310187297170529, 11.49999999999998934 ) ) ;
#77724=CARTESIAN_POINT ( 'NONE',  ( 7.506095096478735407, 19.11734572241606145, -1.500000000000002220 ) ) ;
#77726=EDGE_LOOP ( 'NONE', ( #47488, #77867, #35150, #12851 ) ) ;
#77727=CARTESIAN_POINT ( 'NONE',  ( -88.58953762381671027, -23.47596703998600631, 11.44779298504227683 ) ) ;
#77728=ORIENTED_EDGE ( 'NONE', *, *, #98783, .F. ) ;
#77729=CARTESIAN_POINT ( 'NONE',  ( -88.62287095715004170, -24.64965695001469115, 8.947790433994180503 ) ) ;
#77730=CARTESIAN_POINT ( 'NONE',  ( -80.55620429048339304, -23.47593901973091235, -1.443836447539004642 ) ) ;
#77731=EDGE_LOOP ( 'NONE', ( #5198, #55181, #67288, #98981 ) ) ;
#77735=CARTESIAN_POINT ( 'NONE',  ( -50.29668966358368465, -25.03348023436011260, 7.560224540057909337 ) ) ;
#77736=CARTESIAN_POINT ( 'NONE',  ( -68.58780896930441884, -24.35071581493542681, 9.817618358456032368 ) ) ;
#77737=CARTESIAN_POINT ( 'NONE',  ( 17.27521350410721368, -11.31798593588896829, -1.500000000000002220 ) ) ;
#77738=CARTESIAN_POINT ( 'NONE',  ( -18.67883320684159543, -10.89015303950203517, 11.49999999999999645 ) ) ;
#77739=EDGE_LOOP ( 'NONE', ( #21852, #34455, #11129, #16236 ) ) ;
#77741=CARTESIAN_POINT ( 'NONE',  ( -96.52287095715006160, -24.64965694238575011, 8.947790433994194714 ) ) ;
#77742=CARTESIAN_POINT ( 'NONE',  ( -3.695635658436464244, 22.08213133993951161, 11.49999999999998934 ) ) ;
#77743=EDGE_CURVE ( 'NONE', #99569, #44562, #46941, .T. ) ;
#77744=CARTESIAN_POINT ( 'NONE',  ( -67.52287095715006160, -23.47596703998600631, 11.44779298504228748 ) ) ;
#77746=VERTEX_POINT ( 'NONE', #10319 ) ;
#77747=CARTESIAN_POINT ( 'NONE',  ( -100.3670236477657056, -25.31212503800871971, 4.712017573479897692 ) ) ;
#77748=CARTESIAN_POINT ( 'NONE',  ( -35.60239790912048363, -24.15602025860895452, 10.28564288303536856 ) ) ;
#77749=CARTESIAN_POINT ( 'NONE',  ( -17.98194200498208062, 10.70670730041394947, -1.500000000000002220 ) ) ;
#77750=ORIENTED_EDGE ( 'NONE', *, *, #35399, .T. ) ;
#77753=DIRECTION ( 'NONE',  ( 0.000000000000000000, -2.173523156925979552E-06, 0.9999999999976378895 ) ) ;
#77756=CARTESIAN_POINT ( 'NONE',  ( 20.45381123341165619, -5.387677532796200097, -1.500000000000002220 ) ) ;
#77757=VERTEX_POINT ( 'NONE', #13299 ) ;
#77758=CARTESIAN_POINT ( 'NONE',  ( -50.57159316625579493, -23.48783264082477018, -1.443836473390096797 ) ) ;
#77759=CARTESIAN_POINT ( 'NONE',  ( -0.2038501785326352067, 21.78777694363981254, 11.49999999999998934 ) ) ;
#77763=CARTESIAN_POINT ( 'NONE',  ( -75.55620429048340725, -25.00158670708909625, 2.256160236439166855 ) ) ;
#77764=CARTESIAN_POINT ( 'NONE',  ( -3.523925741820590929, 21.50064390955241578, -1.500000000000002220 ) ) ;
#77771=AXIS2_PLACEMENT_3D ( 'NONE', #1757, #32694, #41832 ) ;
#77772=EDGE_LOOP ( 'NONE', ( #71887, #83005, #17379, #42080 ) ) ;
#77775=AXIS2_PLACEMENT_3D ( 'NONE', #75724, #19455, #44806 ) ;
#77776=CARTESIAN_POINT ( 'NONE',  ( -63.55620429048339304, -23.48783264082478084, -1.443836473390068820 ) ) ;
#77777=CARTESIAN_POINT ( 'NONE',  ( 21.18767802922067034, -0.7184367399587067160, 11.49999999999998934 ) ) ;
#77778=CARTESIAN_POINT ( 'NONE',  ( -125.5562042904833930, -23.47593901973091235, -1.443836447538995760 ) ) ;
#77779=CARTESIAN_POINT ( 'NONE',  ( -95.62287095715002749, -24.91570333823099759, 8.075032458375547506 ) ) ;
#77780=CARTESIAN_POINT ( 'NONE',  ( -81.62287095715005592, -29.50248528299804818, 1.056150453629038477 ) ) ;
#77781=B_SPLINE_CURVE_WITH_KNOTS ( 'NONE', 3,
 ( #62833, #47597, #9519, #93749 ),
 .UNSPECIFIED., .F., .F.,
 ( 4, 4 ),
 ( 0.7893427479188557250, 0.7903434949596209735 ),
 .UNSPECIFIED. ) ;
#77783=AXIS2_PLACEMENT_3D ( 'NONE', #18407, #2694, #33637 ) ;
#77784=CARTESIAN_POINT ( 'NONE',  ( 11.20917403917954225, 15.81763734437701885, -1.500000000000002220 ) ) ;
#77785=CARTESIAN_POINT ( 'NONE',  ( -51.93149462243455616, -25.25905089634592571, 6.174051128686508072 ) ) ;
#77786=VERTEX_POINT ( 'NONE', #96061 ) ;
#77787=AXIS2_PLACEMENT_3D ( 'NONE', #43522, #11555, #56764 ) ;
#77788=CARTESIAN_POINT ( 'NONE',  ( 19.43689267596983683, 0.5339526363925560792, 11.49999999999999645 ) ) ;
#77791=ORIENTED_EDGE ( 'NONE', *, *, #21737, .T. ) ;
#77794=CARTESIAN_POINT ( 'NONE',  ( -64.62287095715005592, -24.64898659630528499, 1.056161002820822592 ) ) ;
#77795=CARTESIAN_POINT ( 'NONE',  ( -93.62566436713133555, -24.51419770103157703, 9.386484678747164523 ) ) ;
#77796=CARTESIAN_POINT ( 'NONE',  ( 14.19269941865516671, -13.59168563846684563, 11.49999999999998934 ) ) ;
#77799=CARTESIAN_POINT ( 'NONE',  ( 20.63042821663210091, 6.393326493806346100, 11.49999999999998934 ) ) ;
#77802=CARTESIAN_POINT ( 'NONE',  ( -21.75560140871883164, 7.562747417745157463, -1.500000000000002220 ) ) ;
#77804=CARTESIAN_POINT ( 'NONE',  ( -55.92287095715006018, -23.47596703998600631, 11.44779298504227683 ) ) ;
#77805=DIRECTION ( 'NONE',  ( 1.000000000000000000, 3.773278334444166432E-23, 8.201307841325785021E-29 ) ) ;
#77806=CARTESIAN_POINT ( 'NONE',  ( -43.62287095715004881, -29.50248528299804818, 1.056150453629031594 ) ) ;
#77807=CARTESIAN_POINT ( 'NONE',  ( -64.62287095715005592, -23.73934037231756733, 11.05740245334329153 ) ) ;
#77809=CARTESIAN_POINT ( 'NONE',  ( -111.7736932848194726, -25.10921665464774577, 4.173604445294007093 ) ) ;
#77811=CARTESIAN_POINT ( 'NONE',  ( -99.32787325113280019, -25.26400820985182705, 4.639922590201173591 ) ) ;
#77812=CARTESIAN_POINT ( 'NONE',  ( 2.793900936927258272, 19.68708943014846469, -1.500000000000002220 ) ) ;
#77813=B_SPLINE_CURVE_WITH_KNOTS ( 'NONE', 3,
 ( #72245, #96562, #98937, #65155 ),
 .UNSPECIFIED., .F., .F.,
 ( 4, 4 ),
 ( 0.000000000000000000, 9.999999999997510880E-05 ),
 .UNSPECIFIED. ) ;
#77814=EDGE_CURVE ( 'NONE', #67032, #46870, #23924, .T. ) ;
#77815=CARTESIAN_POINT ( 'NONE',  ( -72.62287095715005592, -23.47596703998600631, 11.44779298504227860 ) ) ;
#77816=CARTESIAN_POINT ( 'NONE',  ( 9.833179757865110560, 17.22857952739193266, -1.500000000000002220 ) ) ;
#77817=CARTESIAN_POINT ( 'NONE',  ( -94.62287095715005592, -24.66019654487199730, 8.947790411086126383 ) ) ;
#77818=EDGE_CURVE ( 'NONE', #71054, #39828, #66136, .T. ) ;
#77819=ADVANCED_FACE ( 'NONE', ( #11324 ), #530, .T. ) ;
#77820=CARTESIAN_POINT ( 'NONE',  ( -108.5228709571500616, -24.64898659630528854, 1.056161002820831474 ) ) ;
#77821=B_SPLINE_CURVE_WITH_KNOTS ( 'NONE', 3,
 ( #21012, #4807, #51982, #12402, #96645, #27145, #66731, #97153, #82910, #97642, #19518, #83410 ),
 .UNSPECIFIED., .F., .F.,
 ( 4, 2, 2, 2, 2, 4 ),
 ( 0.000000000000000000, 0.0002976555682062342022, 0.0005953111364124684043, 0.0008929667046187024981, 0.001041794488721820792, 0.001190622272824939194 ),
 .UNSPECIFIED. ) ;
#77823=CARTESIAN_POINT ( 'NONE',  ( 8.872108392497455753, -18.76566404461018678, 11.49999999999999645 ) ) ;
#77825=EDGE_CURVE ( 'NONE', #86594, #60374, #15283, .T. ) ;
#77826=VECTOR ( 'NONE', #9385, 1000.000000000000114 ) ;
#77827=CARTESIAN_POINT ( 'NONE',  ( -106.5141348546935802, -24.34968618360934300, 0.1864209137778878034 ) ) ;
#77828=CARTESIAN_POINT ( 'NONE',  ( 20.43669262517703800, -10.12641136740851699, 11.49999999999999645 ) ) ;
#77829=ORIENTED_EDGE ( 'NONE', *, *, #58109, .T. ) ;
#77830=CARTESIAN_POINT ( 'NONE',  ( -69.62363796276726191, -24.65952944569304606, 1.056160979905704567 ) ) ;
#77831=CARTESIAN_POINT ( 'NONE',  ( -69.55367693329765189, -25.17615986935216199, 6.773585123431198340 ) ) ;
#77833=CARTESIAN_POINT ( 'NONE',  ( 19.32837167043147986, -5.866312143582237404, 11.49999999999998934 ) ) ;
#77834=ADVANCED_FACE ( 'NONE', ( #4711 ), #58015, .F. ) ;
#77838=VERTEX_POINT ( 'NONE', #88948 ) ;
#77840=CARTESIAN_POINT ( 'NONE',  ( -7.509321099650855480, 21.62252279970214985, 11.49999999999998934 ) ) ;
#77841=FACE_OUTER_BOUND ( 'NONE', #77234, .T. ) ;
#77843=CARTESIAN_POINT ( 'NONE',  ( -21.57582672592670292, -1.461774377805347802, -1.500000000000002220 ) ) ;
#77845=CARTESIAN_POINT ( 'NONE',  ( -10.06633388967972209, 18.29571535785830960, 11.49999999999999645 ) ) ;
#77846=EDGE_LOOP ( 'NONE', ( #87321, #72792, #74654, #66345 ) ) ;
#77847=VECTOR ( 'NONE', #27977, 1000.000000000000114 ) ;
#77848=CARTESIAN_POINT ( 'NONE',  ( -122.6228709571500417, -24.66019654487199730, 8.947790411086121054 ) ) ;
#77849=CARTESIAN_POINT ( 'NONE',  ( -107.5228709571501042, -23.47593901973090524, -1.443836447538996426 ) ) ;
#77850=CARTESIAN_POINT ( 'NONE',  ( -2.093881351098874521, -21.91542971883435698, 11.49999999999998934 ) ) ;
#77853=CARTESIAN_POINT ( 'NONE',  ( -65.62287095715005592, -23.47596703998600631, 11.44779298504227683 ) ) ;
#77854=ORIENTED_EDGE ( 'NONE', *, *, #70914, .T. ) ;
#77856=CARTESIAN_POINT ( 'NONE',  ( -85.62287095715005592, -23.47593901973091235, -1.443836447539002865 ) ) ;
#77858=LINE ( 'NONE', #22567, #71290 ) ;
#77859=B_SPLINE_CURVE_WITH_KNOTS ( 'NONE', 3,
 ( #9434, #34289, #18052, #24652, #57139, #48014 ),
 .UNSPECIFIED., .F., .F.,
 ( 4, 2, 4 ),
 ( 1.570755371633875854E-05, 0.001396183895866086235, 0.002776660238015833410 ),
 .UNSPECIFIED. ) ;
#77861=EDGE_LOOP ( 'NONE', ( #66274, #23038, #27642, #87548 ) ) ;
#77862=CARTESIAN_POINT ( 'NONE',  ( -71.49851612826357439, -24.51419770103159124, 9.386484678747166299 ) ) ;
#77863=CARTESIAN_POINT ( 'NONE',  ( -101.3783285514244028, -25.10935884294595866, 3.208886314311354848 ) ) ;
#77864=CARTESIAN_POINT ( 'NONE',  ( -100.5228709571500900, -23.84081130425357387, 10.88220057483161085 ) ) ;
#77865=CARTESIAN_POINT ( 'NONE',  ( -2.750569593922542300, -20.27526743851804625, -1.500000000000002220 ) ) ;
#77866=ADVANCED_FACE ( 'NONE', ( #19428 ), #71055, .T. ) ;
#77867=ORIENTED_EDGE ( 'NONE', *, *, #6016, .F. ) ;
#77868=CARTESIAN_POINT ( 'NONE',  ( -100.0587518433314784, -25.30258194450249931, 5.273723563230666933 ) ) ;
#77869=CARTESIAN_POINT ( 'NONE',  ( -44.66287493451820012, -23.48783264082476663, -1.443836473390094799 ) ) ;
#77871=CARTESIAN_POINT ( 'NONE',  ( -22.23078454666273274, -1.437644496696519170, -1.500000000000002220 ) ) ;
#77873=CARTESIAN_POINT ( 'NONE',  ( -55.52287095715004028, -24.52323809116984066, 9.355190652339430812 ) ) ;
#77875=ORIENTED_EDGE ( 'NONE', *, *, #82922, .T. ) ;
#77876=CARTESIAN_POINT ( 'NONE',  ( -44.52287095715004739, -23.48783264082477018, -1.443836473390094577 ) ) ;
#77877=CARTESIAN_POINT ( 'NONE',  ( -118.6228709571500559, -29.50248528299804818, 1.056150453629045360 ) ) ;
#77878=CARTESIAN_POINT ( 'NONE',  ( 12.46380520747237419, 16.70348211664046900, 11.49999999999998934 ) ) ;
#77879=EDGE_LOOP ( 'NONE', ( #56657, #68193, #72456, #49951 ) ) ;
#77881=ORIENTED_EDGE ( 'NONE', *, *, #39916, .F. ) ;
#77883=CARTESIAN_POINT ( 'NONE',  ( -58.52287095715006160, -24.50321055353803601, 9.387540953477515160 ) ) ;
#77884=CARTESIAN_POINT ( 'NONE',  ( 14.98681507544721292, -14.71779577663021321, -1.500000000000002220 ) ) ;
#77885=EDGE_CURVE ( 'NONE', #503, #8654, #23737, .T. ) ;
#77886=ORIENTED_EDGE ( 'NONE', *, *, #84341, .F. ) ;
#77887=CARTESIAN_POINT ( 'NONE',  ( -90.52287095715006160, -24.99132157543165889, 2.256160258750667502 ) ) ;
#77888=CARTESIAN_POINT ( 'NONE',  ( -50.38191529551148307, -25.10935757153401937, 2.832404819425170306 ) ) ;
#77890=CARTESIAN_POINT ( 'NONE',  ( -49.52287095715006160, -29.50250243563736774, 8.947779886222146928 ) ) ;
#77891=PLANE ( 'NONE',  #67581 ) ;
#77893=CARTESIAN_POINT ( 'NONE',  ( -12.04397493737346991, 18.63154960201688226, 11.49999999999999645 ) ) ;
#77895=DIRECTION ( 'NONE',  ( -3.773278334453079618E-23, 0.9999999999976377785, 2.173523156925979975E-06 ) ) ;
#77896=EDGE_CURVE ( 'NONE', #95483, #477, #63655, .T. ) ;
#77898=ORIENTED_EDGE ( 'NONE', *, *, #45291, .F. ) ;
#77899=CARTESIAN_POINT ( 'NONE',  ( -21.51096707683950626, -7.176001652309477841, -1.500000000000002220 ) ) ;
#77900=CARTESIAN_POINT ( 'NONE',  ( -111.5228709571499763, -23.73934037231757443, 11.05740245334327909 ) ) ;
#77901=VERTEX_POINT ( 'NONE', #22894 ) ;
#77902=EDGE_LOOP ( 'NONE', ( #83608, #11279, #52698, #81621 ) ) ;
#77903=LINE ( 'NONE', #8410, #32059 ) ;
#77904=AXIS2_PLACEMENT_3D ( 'NONE', #69794, #60199, #6398 ) ;
#77906=CARTESIAN_POINT ( 'NONE',  ( 13.66866334921533799, -14.80927461459226890, 11.49999999999998934 ) ) ;
#77908=VERTEX_POINT ( 'NONE', #44773 ) ;
#77909=DIRECTION ( 'NONE',  ( 0.000000000000000000, -2.173523156925979552E-06, 0.9999999999976378895 ) ) ;
#77910=CARTESIAN_POINT ( 'NONE',  ( 7.974090105135403839, 20.87195307945309963, -1.500000000000002220 ) ) ;
#77912=CARTESIAN_POINT ( 'NONE',  ( -104.5118022433312461, -24.51314013834316086, 0.6176544820404171743 ) ) ;
#77913=CARTESIAN_POINT ( 'NONE',  ( -101.2523990460597503, -25.25341228077052946, 6.807413982353327064 ) ) ;
#77914=DIRECTION ( 'NONE',  ( -1.000000000000000000, -3.773278334444166432E-23, -8.201307841325785021E-29 ) ) ;
#77915=LINE ( 'NONE', #53117, #63544 ) ;
#77916=CARTESIAN_POINT ( 'NONE',  ( -38.62287095715005592, -24.65952944569303895, 1.056160979905692798 ) ) ;
#77917=CARTESIAN_POINT ( 'NONE',  ( -130.5728709571500588, -24.37807914296826084, 0.3010598746230577771 ) ) ;
#77919=CARTESIAN_POINT ( 'NONE',  ( -9.112395119859147741, -17.30902560603237106, 11.49999999999998934 ) ) ;
#77921=CARTESIAN_POINT ( 'NONE',  ( 21.44729954461699251, -1.519088741117538000, 11.49999999999998934 ) ) ;
#77922=CARTESIAN_POINT ( 'NONE',  ( -95.62287095715005592, -23.47596703998600631, 11.44779298504227860 ) ) ;
#77926=CARTESIAN_POINT ( 'NONE',  ( -22.79553223295561892, 1.966428799096173075, -1.500000000000002220 ) ) ;
#77929=CARTESIAN_POINT ( 'NONE',  ( -53.65126712112351015, -23.73766607897669090, -1.055555164236459564 ) ) ;
#77930=CARTESIAN_POINT ( 'NONE',  ( -5.935188749463110369, 19.13178230186815298, 11.49999999999999645 ) ) ;
#77931=CARTESIAN_POINT ( 'NONE',  ( -99.62287095715005592, -23.47593901973091235, -1.443836447539001089 ) ) ;
#77932=LINE ( 'NONE', #56137, #3111 ) ;
#77936=ORIENTED_EDGE ( 'NONE', *, *, #17456, .F. ) ;
#77937=CARTESIAN_POINT ( 'NONE',  ( -33.62287095715005592, -24.66019654487199020, 8.947790411086138818 ) ) ;
#77938=CARTESIAN_POINT ( 'NONE',  ( -7.892909027492730267, -20.28523913882780505, 11.49999999999998934 ) ) ;
#77939=DIRECTION ( 'NONE',  ( -3.773278334444167608E-23, 1.000000000000000000, 0.000000000000000000 ) ) ;
#77940=CARTESIAN_POINT ( 'NONE',  ( -14.15603575923578283, -13.64839490926926580, -1.500000000000002220 ) ) ;
#77941=CARTESIAN_POINT ( 'NONE',  ( -38.62287095715005592, -23.48786465467240703, 11.44779295918255180 ) ) ;
#77942=CARTESIAN_POINT ( 'NONE',  ( -110.0852742341990904, -25.27925937390634914, 5.455857480927421399 ) ) ;
#77945=CARTESIAN_POINT ( 'NONE',  ( -91.64133805002603594, -23.48786465467241058, 11.44779295918254469 ) ) ;
#77947=CARTESIAN_POINT ( 'NONE',  ( 15.21836549854886123, 13.79734045396011943, 11.49999999999999645 ) ) ;
#77951=CARTESIAN_POINT ( 'NONE',  ( -22.11960324842224423, 4.537628740662121629, 11.49999999999999645 ) ) ;
#77953=CARTESIAN_POINT ( 'NONE',  ( -99.65355524409876864, -25.26387372658618347, 4.362766323930155288 ) ) ;
#77954=CARTESIAN_POINT ( 'NONE',  ( -27.37821967320581251, -24.79341979850518385, 7.571465340039231329 ) ) ;
#77955=CARTESIAN_POINT ( 'NONE',  ( -125.5569696030716926, -23.48786465467241769, 11.44779295918253581 ) ) ;
#77958=CARTESIAN_POINT ( 'NONE',  ( -26.25023971703978276, -24.93063488596019539, 7.578546381800906673 ) ) ;
#77961=CARTESIAN_POINT ( 'NONE',  ( -18.27982475084466785, -14.08179083545084964, 11.49999999999999645 ) ) ;
#77962=CARTESIAN_POINT ( 'NONE',  ( 16.42120958226126604, -15.83219868413775622, 11.49999999999998934 ) ) ;
#77963=CARTESIAN_POINT ( 'NONE',  ( -104.5228709571500758, -23.47593901973090524, -1.443836447538996204 ) ) ;
#77966=CARTESIAN_POINT ( 'NONE',  ( 22.01961411883556252, 4.383451955130949429, 11.49999999999999645 ) ) ;
#77967=ORIENTED_EDGE ( 'NONE', *, *, #79791, .F. ) ;
#77969=CARTESIAN_POINT ( 'NONE',  ( -43.52287095715007581, -23.72773821059536203, 11.05748984161097503 ) ) ;
#77971=CARTESIAN_POINT ( 'NONE',  ( 20.73430856240977249, 7.200853762728330665, -1.500000000000002220 ) ) ;
#77972=B_SPLINE_CURVE_WITH_KNOTS ( 'NONE', 3,
 ( #47481, #69312, #23617, #15016 ),
 .UNSPECIFIED., .F., .F.,
 ( 4, 4 ),
 ( 0.6209434004830697296, 0.6299498317551853743 ),
 .UNSPECIFIED. ) ;
#77974=CARTESIAN_POINT ( 'NONE',  ( -34.57050063697510467, -23.48786465467240347, 11.44779295918255535 ) ) ;
#77975=CARTESIAN_POINT ( 'NONE',  ( -70.62287095715005592, -29.50250243563736774, 8.947779886222143375 ) ) ;
#77976=ORIENTED_EDGE ( 'NONE', *, *, #67096, .T. ) ;
#77977=DIRECTION ( 'NONE',  ( -3.773278334453079618E-23, 0.9999999999976377785, 2.173523156925979975E-06 ) ) ;
#77980=CARTESIAN_POINT ( 'NONE',  ( 13.99439195134931069, 14.96789054323355828, 11.49999999999998934 ) ) ;
#77981=ORIENTED_EDGE ( 'NONE', *, *, #64252, .T. ) ;
#77983=VERTEX_POINT ( 'NONE', #7697 ) ;
#77984=ORIENTED_EDGE ( 'NONE', *, *, #776, .T. ) ;
#77985=B_SPLINE_CURVE_WITH_KNOTS ( 'NONE', 3,
 ( #57984, #65106, #66334, #83015 ),
 .UNSPECIFIED., .F., .F.,
 ( 4, 4 ),
 ( 0.000000000000000000, 1.000000000000000000 ),
 .UNSPECIFIED. ) ;
#77986=CARTESIAN_POINT ( 'NONE',  ( 5.395019145045520048, -22.42585393411717121, -1.500000000000002220 ) ) ;
#77987=CARTESIAN_POINT ( 'NONE',  ( -112.5228709571500474, -23.73934037231757443, 11.05740245334328087 ) ) ;
#77988=CARTESIAN_POINT ( 'NONE',  ( -6.888417027594036846, 19.07602104198033643, -1.500000000000002220 ) ) ;
#77989=ORIENTED_EDGE ( 'NONE', *, *, #64578, .F. ) ;
#77990=DIRECTION ( 'NONE',  ( 1.000000000000000000, 3.773278334444167608E-23, 8.201307833595939069E-29 ) ) ;
#77991=CARTESIAN_POINT ( 'NONE',  ( -92.51515423418101136, -23.96119346886881374, -0.6495511937831873750 ) ) ;
#77992=EDGE_CURVE ( 'NONE', #27734, #31312, #40648, .T. ) ;
#77996=CARTESIAN_POINT ( 'NONE',  ( -19.15072323977689095, -9.709862252083167888, 11.49999999999999645 ) ) ;
#77998=CARTESIAN_POINT ( 'NONE',  ( -75.55242436766256731, -24.15503026093913519, -0.2815557561904521444 ) ) ;
#78002=CARTESIAN_POINT ( 'NONE',  ( 1.902724757927627408, 20.64897553884969028, -1.500000000000002220 ) ) ;
#78003=VERTEX_POINT ( 'NONE', #38642 ) ;
#78005=EDGE_LOOP ( 'NONE', ( #86768, #13843, #74288, #97122 ) ) ;
#78006=EDGE_CURVE ( 'NONE', #42298, #59704, #52864, .T. ) ;
#78007=CARTESIAN_POINT ( 'NONE',  ( -41.53388201844860106, -24.51419770103157347, 9.386484678747180510 ) ) ;
#78011=CARTESIAN_POINT ( 'NONE',  ( -40.52287095715005449, -23.48783264082476308, -1.443836473390097908 ) ) ;
#78012=CARTESIAN_POINT ( 'NONE',  ( -42.63428171904830322, -24.35071581493543036, 9.817618358456037697 ) ) ;
#78013=CARTESIAN_POINT ( 'NONE',  ( -28.34221723987227293, -24.69535842467096032, 1.737203919470178271 ) ) ;
#78014=CARTESIAN_POINT ( 'NONE',  ( 19.60348439636399931, 10.09110264789753053, 11.49999999999999645 ) ) ;
#78016=CARTESIAN_POINT ( 'NONE',  ( 11.64696156460271581, 19.30390316350253244, -1.500000000000002220 ) ) ;
#78017=CARTESIAN_POINT ( 'NONE',  ( 2.184583272949580213, -20.89682302726931340, 11.49999999999998934 ) ) ;
#78022=FACE_OUTER_BOUND ( 'NONE', #65907, .T. ) ;
#78024=VECTOR ( 'NONE', #81423, 1000.000000000000114 ) ;
#78027=CARTESIAN_POINT ( 'NONE',  ( -3.044128750896296420, -20.94304649679510888, -1.500000000000002220 ) ) ;
#78028=CARTESIAN_POINT ( 'NONE',  ( -126.6228709571500275, -23.48783264082479505, -1.443836473390057051 ) ) ;
#78029=CARTESIAN_POINT ( 'NONE',  ( -59.79865720102922921, -25.03722704563418944, 7.590184509431679771 ) ) ;
#78030=CARTESIAN_POINT ( 'NONE',  ( -88.62287095715002749, -24.50321055353805377, 9.387540953477525818 ) ) ;
#78032=CARTESIAN_POINT ( 'NONE',  ( -81.52287095715010423, -23.47593901973090524, -1.443836447538996648 ) ) ;
#78033=CARTESIAN_POINT ( 'NONE',  ( 19.81268554055766273, 9.900562300003143079, -1.500000000000002220 ) ) ;
#78034=CARTESIAN_POINT ( 'NONE',  ( -71.59683346284329275, -23.96119346886880308, -0.6495511937832095795 ) ) ;
#78035=ORIENTED_EDGE ( 'NONE', *, *, #70046, .F. ) ;
#78037=CARTESIAN_POINT ( 'NONE',  ( -37.51296537665867703, -23.73766607897670866, -1.055555164236442245 ) ) ;
#78038=CARTESIAN_POINT ( 'NONE',  ( -40.37291966744255234, -25.30367284796214378, 5.540795143838759707 ) ) ;
#78043=CARTESIAN_POINT ( 'NONE',  ( -0.2416374764669896869, -19.45557994585427508, -1.500000000000002220 ) ) ;
#78045=CARTESIAN_POINT ( 'NONE',  ( 20.92345209525186078, -4.499874906010187026, -1.500000000000002220 ) ) ;
#78046=CARTESIAN_POINT ( 'NONE',  ( -38.52287095715009713, -23.96177878511310055, 10.65340807706330573 ) ) ;
#78049=CARTESIAN_POINT ( 'NONE',  ( -51.50150689877243337, -24.15543982623907127, -0.2315651400026664530 ) ) ;
#78051=CARTESIAN_POINT ( 'NONE',  ( -22.63693132222386950, 1.387278323242118416, -1.500000000000002220 ) ) ;
#78052=B_SPLINE_CURVE_WITH_KNOTS ( 'NONE', 3,
 ( #27916, #11682, #65512, #89815, #96432, #20285, #51259, #89321, #66999, #26922, #5574, #19790, #82198, #13174, #81708, #81206, #73106, #44145, #42665, #20785, #97911, #42168, #12683, #90314, #28404, #59371, #43646, #35041, #96932, #73598, #74584, #43156, #5074, #4593, #36024, #66512, #82693, #36519, #67485, #98409, #90814, #99412, #60386, #53762, #67988, #6071, #84188, #38021, #83692, #46144, #45149, #21778, #75571, #6574, #84691, #39020, #44643, #98912, #69972, #15683, #15179, #37026, #92800, #69476, #7072, #92304, #77570, #77068, #60874, #7573, #457, #23792, #29906, #22277, #14679, #31413, #22774, #52754, #54264, #68971, #62370, #29405, #100395, #14173, #76075, #13671, #53261, #93298, #91801, #45642, #38522, #76566, #83186, #30908, #99896, #37525, #61875, #61377, #91309, #68479, #30407, #23281, #85193, #46650, #8073, #47150, #56773, #54765, #87199, #1977, #95313, #95807, #47652, #55770, #79077, #17688, #10570, #24301, #32416, #86695, #33406, #25802, #63894, #63389, #80087, #16682, #86199, #48662, #17182, #9575, #41533, #25295, #8581, #32920, #55267, #64897, #41037, #40027, #85703, #78566, #16182, #78067, #40539, #18188, #2981, #87704, #62890, #71489, #39528, #964, #72487, #70480, #93809, #9074, #64398, #31917, #79585, #49161, #48153, #94807, #33915, #94303, #71992, #70986, #1476, #24791, #56275, #10075, #2473, #96810, #43531, #82083, #50147, #26800, #82576, #88706, #57763, #74468, #90192, #26303, #4960, #12567, #11564, #36406, #19176, #88209, #35906, #66874, #97800, #73975, #35423, #57278, #27795, #28292, #13056, #58261, #20671, #97311, #51639, #42044, #81088, #51135, #59251, #27302, #89203, #44017, #74949, #5454, #67367, #19672, #66383, #96313, #18677, #49651, #43033, #42542, #80584, #12062, #11076, #4474, #58748, #72988, #3477, #34415, #73477, #89700, #65396, #50637, #3974, #34915, #65889, #81591, #20174, #84569, #22158, #6950, #92676, #68855, #75951, #99773, #15555, #52632, #44524, #45528, #75448, #61259, #60260, #37904, #91678, #5948, #98286, #21169, #15056, #98793, #91183, #28793, #68359, #46516, #14051, #99292, #30280, #46027, #59758, #76946, #83059, #92181, #29789, #30790, #29289, #6456, #53145, #7442, #67867, #69353, #13554, #90691, #100270, #52136, #22655, #76447, #38397, #60756, #14559, #53645, #61758, #84071, #23154, #54146, #85069, #77445, #36904, #7947, #38898, #37413, #21658, #83567, #45032, #1849, #17058, #9951, #10447, #86574, #48025, #48533, #94178, #79459, #87074, #17565, #24663, #62252, #40903, #78950, #47524, #95191, #31792, #838, #32787, #1352, #55643, #56647, #40408, #33281, #69858, #71864, #70861, #93176, #2353, #9449, #64269, #25675, #337, #71361, #87579, #18063, #49031, #77940, #63769, #79960, #16052, #31283, #23663, #54635, #85569, #24169, #47023, #55141, #8453, #39400, #78448, #86074, #8950, #56144, #70354, #16548, #62761, #39898, #32287, #25169, #63257, #93679, #94683, #33792, #58144, #81474, #57644, #97189, #64776, #35794, #88585, #19557, #43415, #11450, #18560, #2860, #74350, #95691, #51023, #27684, #65768, #50516, #66766, #58633, #89579, #89081, #34299, #96198, #88088, #11948, #49534, #4352, #3365, #42915, #34797, #80464, #41409, #26177, #20061, #41923, #65275, #72364, #42429, #57151, #10956, #73361, #96683, #81964, #72865, #12445, #26685, #35303, #3856, #4841, #19058, #50032, #27185, #97684, #80967, #28180, #73854, #66266, #59138, #90077, #20548, #82456, #51522, #21540, #29168, #52516, #99655, #12937, #60143, #59637, #83447, #91066, #68737, #13937, #30161, #61135, #36789, #13437, #76325, #44910, #92062, #36295, #7317, #75834, #91561, #14929, #6332, #90569, #74837, #45903, #67251, #22532, #53525, #37288, #22039, #38272, #83952, #68239, #14433, #5833, #67752, #21048, #60640, #52017, #6825, #75335, #53022, #99168, #82946, #43904, #98173, #84448, #44411, #98671, #5335, #29667, #61636, #45407, #37783, #76819, #69229, #28675, #100145, #30667, #92556, #23028, #54018, #85442, #62629, #78325, #1723, #54509, #56019, #69736, #77323, #86949, #84947, #16936, #32159, #711, #85953, #1225, #63132, #63638, #8830, #94559, #32661, #25044, #39767, #7824, #17437, #94058, #93548, #9827, #46896, #15929, #47900, #16426, #70730, #55517, #38771, #24544, #77816, #95067, #71236, #70231, #25553, #8326, #46392, #40281, #48400, #79333, #86451, #78819, #15431, #9316, #40777, #71739, #47399, #214, #23531, #39271, #2232, #31159, #33161, #64145, #62129, #93051, #31658, #24042, #55015, #41282, #18933, #2732, #3730, #57022, #80846, #26564, #72238, #34174, #33669, #64650, #96070, #80338, #95565, #42308, #10329, #48905, #65145, #57523, #27059, #87452, #58022, #26049, #34674, #88460, #11823, #87960, #10832, #50400, #58516, #18439, #49912, #89453, #49412, #17944, #41798, #79831, #81342, #72741, #11331, #73237, #65644, #88960, #96558, #19435, #42794, #73726, #4221, #35175, #3241, #66144, #97061, #27564, #56522, #48742, #47224, #2558, #8661, #78146, #63979, #10162, #46726, #94889, #47729, #39097, #17778, #24874, #79663, #2065, #25381, #33004, #94392, #55850, #77652, #48232, #41121, #33495, #78645, #72078, #17269, #64482, #62452, #1051, #56358, #31993, #87790, #25886, #55347, #71572, #95396, #56858, #9151, #86778, #16266, #8159, #70054, #63470, #39603, #540, #32498, #31488, #79163, #9662, #62963, #87277, #93379, #23867, #93890, #54843, #85784, #70555, #24378, #40618, #86279, #1558, #40112, #16759, #71068, #3263, #71257, #39798, #78845, #1254, #49435, #25067, #9848, #25576, #56549, #41308, #65173, #9345, #86970, #40800, #87985, #33697, #47924, #72768, #17462, #34202, #48426, #10859, #40308, #96099, #1747, #32685, #26077, #26588, #8850, #18961, #95590, #94586, #49940, #63664, #70756, #64675, #57050, #18463, #87477, #17970, #32182, #10352, #80368, #57548, #71762, #88487, #79857, #63155, #24566, #94082, #41823, #55543, #2254, #33188, #86474, #16960, #56045, #79356, #64170, #48929, #95091, #72268, #2756, #97582, #81366, #3756, #66670, #73263, #28083, #42819, #19456, #34698, #4249, #82357, #36686, #42330, #65669, #67651, #13332, #51421, #27083, #35695, #74251, #50423, #90967, #20449, #59533, #67158, #36193, #98570, #21437, #27587, #19954, #81864, #29066, #89975, #11848, #51920, #4745, #60039, #12343, #58049, #88986, #43313, #97088, #73750, #12836, #96585, #35198, #43805, #58538, #80870, #74737, #59037, #66170, #5236, #98066, #11357, #89478, #50926, #20948, #28573, #90473, #82849, #44312, #75239, #5731, #69125, #100049, #84848, #8234, #21934, #30057, #53417, #31055, #77220, #91455, #15831, #61031, #46799, #91962, #54410, #52919, #39174, #14329, #83851, #69638, #77721, #52415, #84345, #44807, #23427, #30563, #85345, #70129, #83348, #76716, #616, #31562, #92952, #60540, #7217, #62524, #99064, #93454, #13832, #45306, #76227, #62027, #75725, #37678, #6228, #37184, #22434, #68637, #14828, #38673, #68140, #99555, #29562, #45796, #38166, #7726, #61535, #116, #6725, #92452, #22924, #15327, #53915, #46291, #47301, #19711, #40187, #3515, #27345, #94467, #1126, #85857, #58305, #78226, #34955, #11607, #49697, #34460, #50684, #96354, #1633, #26842, #16840, #78719, #70630, #73029, #32064, #88752, #86358, #65435, #17344, #63038, #23947, #8736, #42584, #24451, #47800, #54914, #24949, #74019, #71140, #55925, #80627, #73521, #16335, #4011, #39674, #19220, #86847, #89242, #55419, #32565, #11114, #65930, #93960, #9223, #81630, #42084, #12104, #63545, #57806, #50187, #81126, #43074, #96850, #4514, #35461, #66431, #44567, #37453, #37945, #90238, #98333, #21212, #29333, #53187, #66920, #74998, #28840, #75995, #21705, #35951, #5498, #22203, #59292, #28334, #60304, #59805, #52179, #84118, #67917, #51182, #75494, #97840, #6998, #83615, #82618, #97353, #20713, #58793, #52678, #45075, #60803, #45574, #68404, #5002, #83110, #27838, #43571, #14602, #89744, #51685, #13097, #6503, #20212, #14099, #99336, #90739, #13600, #76491, #29832, #91724, #82125, #44065, #74507, #36447, #67413, #12609, #5996, #36946, #98837, #91228, #69399, #31842, #30835, #7490, #61302, #92719, #70401, #24714, #30328, #53687, #46073, #92228, #1400, #22700, #78495, #55193, #93224, #77988, #63308, #39452, #46564, #889, #86621, #9497, #15601, #7995, #69898, #55693, #8502, #38446, #62300, #15106, #68894, #84618, #86122, #100318, #61800, #99821, #38943, #17107, #85116, #383, #62811, #77493, #48072, #93725, #23713, #23207, #24218, #47074, #54192, #31331, #54684, #16598, #76992, #85615, #16104, #47575, #79000, #8995, #39949, #70909, #32335, #94227, #33328, #95238, #87119, #88134, #17613, #3409, #79509, #11494, #64825, #96733, #41457, #48585, #9997, #2907, #56700, #40953, #11002, #25217, #63817, #72414, #95738, #26728, #1895, #57688, #56195, #34345, #18602, #89129, #50562, #71915, #81015, #81519, #2400, #72912, #34843, #64319, #71408, #25722, #32841, #42471, #87631, #33837, #57201, #49578, #19103, #26227, #18115, #49081, #80511, #50075, #65324, #80008, #3904, #10496, #65812, #41969, #73410, #96244, #27232, #88633, #58187, #19601, #40459, #94730, #60187, #12983, #83494, #90617, #13981, #6381, #42963, #36337, #75881, #60684, #52561, #20103, #67295, #22084, #58675, #29716, #53070, #51069, #82010, #21588, #4398, #36839, #11994, #91607, #20600, #28220, #51569, #98721, #73899, #59180, #89624, #82500, #90121, #67802, #43948, #29219, #91112, #35837, #12495, #75380, #74394, #43460, #35346, #37341, #74881, #21096, #44957, #5384, #4891, #66309, #68285, #99214, #52064, #66808, #97237, #98215, #27727, #28725, #97730, #59685, #82992, #13485, #44453, #5878, #100191, #54067, #93098, #61681, #39818, #54551, #7870, #22574, #15972, #62175, #32201, #94101, #68781, #24088, #24588, #53571, #46942, #78370, #70776, #83997, #77865, #31202, #55059, #14480, #76862, #84991, #38816, #8372, #1273, #84496, #92598, #15476, #62678, #39317, #14978, #47442, #23076, #8872, #45951, #70278, #46437, #69781, #63175, #85489, #37828, #23581, #7364, #45457, #758, #69277, #76371, #38317, #6874, #31711, #93595, #85997, #16470, #99699, #92107, #258, #30204, #61186, #30711, #77369, #94607, #25087, #65192, #47944, #80388, #34220, #56568, #87499, #73280, #10877, #18979, #88503, #17987, #95610, #95110, #33207, #41843, #25598, #72785, #3283, #79377, #56063, #18483, #17483, #86991, #78865, #9870, #57069, #11373, #16978, #40327, #42348, #49958, #26097, #9366, #96116, #26605, #79876, #64695, #80887, #88004, #64189, #49454, #3774, #96601, #2279, #48948, #10370, #57566, #41329, #34713, #65687, #72285, #48447, #2777, #55561, #40820, #33716, #86495, #71279, #71783, #1767, #32706, #63687, #13854, #27100, #59554, #74758, #67670, #68158, #19975, #28100, #51439, #90491, #36705, #44330, #75259, #82376, #19475, #98591, #36211, #4762, #52436, #89494, #58555, #20967, #59057, #12855, #44826, #98085, #81385, #5253, #27606, #37205, #50439, #29085, #67175, #60059, #21457, #58069, #43823, #90986, #75747, #83367, #35216, #28591, #89002, #73767, #6247, #11866, #66188, #97109, #42837, #4267, #12359, #50944, #81882, #35716, #43332, #66689, #13354, #74270, #97600, #89993, #20467, #51938, #82867, #5751, #15849, #54430, #22453, #99575, #62046, #61050, #85364, #21953, #93471, #14849, #77238, #633, #69146, #76247, #60560, #31581, #52938, #8252, #46821, #22945, #7745, #23964, #69657, #76736, #134, #16353, #53438, #45325, #46312, #6744, #92972, #91982, #38691, #92472, #37698, #99084, #83869, #77737, #30080, #84367, #29583, #100067, #47319, #45815, #30583, #31075, #23447, #70147, #54933, #91478, #53936, #62545, #78243, #39191, #68658, #84867, #8754, #7238, #39692, #14349, #38187, #61554, #85876, #15349, #95489, #49333, #49838, #79252, #86867, #9750, #56947, #70651, #17362, #16859, #40705, #48324, #25975, #71659, #87881, #18365, #94484, #71159, #33591, #32584, #9241, #63057, #65072, #2158, #48831, #72662, #33091, #47818, #32081, #3159, #93978, #80265, #10758, #94984, #79757, #95989, #41212, #64070, #72165, #88380, #11253, #25471, #17867, #78740, #64570, #63564, #10250, #56447, #40203, #1143, #24470, #41722, #1649, #24968, #55436, #87372, #18861, #2655, #34100, #26487, #57451, #80771, #86375, #55942, #36089, #43215, #75141, #42721, #19847, #35601, #59430, #11744, #65571, #44209, #4646, #28968, #42229, #74641, #89873, #82752, #83253, #35099, #20343, #20846, #66572, #51823, #90371, #13235, #97485, #34599, #5632, #51317, #50822, #67549, #4147, #73654, #5135, #74153, #27978, #59942, #12734, #96486, #73162, #28465, #36578, #66068, #26977, #98467, #58931, #90870, #3653, #67057, #82257, #21341, #57948, #96988, #43704, #97966, #52319, #88887, #27487, #81763, #19360, #50325, #81261, #58443, #12234, #89377, #76133, #45206, #46198, #45702, #38078, #521, #84754, #68047, #92364, #14231, #77129, #69033, #29461, #99961, #85250, #8143, #44705, #30471, #77631, #62433, #54325, #21841, #61437, #23851, #60444, #31471, #54825, #52816, #83751, #23340, #6130, #38584, #92863, #14735, #93359, #7637, #39080, #46708, #76627, #53821, #6631, #13734, #70034, #22834, #37585, #37083, #15241, #98971, #69544, #24, #29966, #30967, #91365, #75630, #68537, #99467, #60935, #91866, #22337, #61933, #53321, #15743, #7128, #84250, #95870, #25357, #64460, #72053, #41099, #2041, #78624, #40090, #31976, #32983, #72547, #94867, #24359, #56835, #9638, #41602, #86756, #62944, #93868, #48212, #1534, #55326, #56336, #70537, #8641, #17244, #40598, #2537, #47207, #33469, #86260, #17751, #63958, #33975, #26365, #1025, #25861, #16740, #9131, #16246, #55829, #64958, #32474, #79140, #87256, #63448, #3039, #48722, #71548, #47708, #79640, #18250, #71045, #94368, #10135, #95373, #24855, #39585, #87768, #49222, #85760, #78126, #80150, #10640, #97858, #98356, #50208, #58326, #81653, #89763, #66941, #74531, #5022, #12123, #49719, #28352, #66455, #34977, #82638, #19241, #88773, #20234, #89263, #43097, #44088, #27858, #11137, #35483, #57830, #51203, #73052, #74040, #81150, #18740, #12631, #35970, #43591, #4537, #97375, #57338, #58814, #59315, #75017, #19731, #51703, #82145, #13120, #3537, #11627, #90259, #20735, #5515, #36466, #67431, #88268, #80652, #42106, #50703, #34479, #26863, #65456, #96373, #42605, #73541, #4033, #65952, #96874, #27364, #70300, #45097, #21231, #52699, #31732, #86513, #90757, #13618, #16997, #63198, #780, #75516, #85509, #23599, #98859, #40346, #62698, #8893, #16490, #86014, #46963, #21725, #77387, #69797, #31226, #47964, #39338, #67936, #1291, #54571, #78887, #62195, #6015, #93614, #29353, #9387, #55583, #77884, #60328, #52202, #15992, #83130, #24108, #91252, #83638, #44588, #14120, #55081, #71301, #36970, #7887, #28862, #94121, #47462, #38838, #8390, #78389, #276, #59824, #39839, #70800, #32221, #24605, #93118, #42859, #48967, #41348, #2797, #89022, #10897, #40839, #73302, #26119, #58088, #33734, #79398, #9888, #64716, #18005, #71805, #72801, #87013, #72301, #41862, #79897, #19498, #3308, #57090, #2296, #34240, #80405, #50458, #11889, #17505, #42369, #1787, #33226, #65214, #96620, #64207, #32726, #95130, #49475, #3796, #63709, #25619, #95634, #88025, #96138, #81409, #56589, #10390, #18501, #80904, #26625, #87525, #65707, #57586, #27122, #88523, #34735, #18998, #49977, #94625, #11392, #56081, #25106, #48469, #36727, #98109, #89514, #28615, #74291, #35237, #29104, #21477, #60080, #20986, #82888, #73788, #75277, #44845, #19999, #91497, #14370, #12381, #43354, #83387, #66208, #98612, #52455, #59578, #60580, #21975, #67693, #37226, #6269, #5273, #52957, #4287, #20489, #12873, #50967, #91004, #35737, #13373, #67194, #81904, #97127, #27627, #13874, #4782, #66708, #58573, #43847, #83888, #90017, #74776, #44351, #51460, #29601, #5770, #97619, #75769, #36231, #68178, #28120, #82395, #90509, #99104, #59080, #51959, #47338, #7765, #32099, #45346, #77756, #92991, #85892, #86393, #38211, #46331, #23982, #69675, #54954, #62567, #93492, #155, #37717, #16372, #54449, #22966, #70670, #7257, #76757, #8270, #77262, #31098, #63073, #15872, #99596, #23468, #31600, #78260, #85383, #53957, #46838, #8773, #39710, #76268, #62067, #1164, #93998, #24487, #53461, #39209, #55454, #92000, #6762, #68676, #84390, #14870, #100087, #30099, #30601, #61072, #22470, #45838, #84886, #69167, #61573, #92496, #15368, #38712, #70168, #652, #72680, #87392, #34118, #3179, #40722, #17381, #79274, #55960, #9261, #71679, #18384, #73181, #78760, #1667, #3671, #49858, #87901, #63581, #72184, #10272, #86889, #26999, #56966, #96010, #65091, #26505, #11269, #9768, #47839, #48344, #40225, #57468, #33109, #17887, #33611, #64593, #88402, #41229, #18877, #80788, #42251, #2673, #71178, #34619, #25994, #95003, #65588, #25495, #96503, #2177, #57966, #64087, #56466, #16876, #32606, #94504, #24985, #48850, #49353, #79775, #95507, #80283, #10777, #41740, #12753, #52335, #97986, #88905, #90392, #59958, #75647, #20361, #83272, #59448, #13750, #4165, #43233, #67567, #74170, #29477, #42739, #44721, #66590, #28986, #75158, #19376, #28484, #58461, #6147, #37099, #5156, #89395, #11763, #74658, #81282, #36106, #20867, #4666, #44227, #73672, #68063, #35616, #67076, #90886, #58954, #66089, #51838, #35116, #43725, #82278, #19868, #98987, #82772, #98485, #5649, #36598, #13254, #81782, #97502, #97004, #21361, #27506, #50342, #50842, #12253, #27997, #89893, #51336, #37603, #68552, #22850, #76642, #99486, #30983, #45223, #83767, #61452, #15257, #46722, #21857, #77648, #76148, #54340, #92379, #93374, #60952, #6647, #536, #70550, #29981, #92877, #38600, #91879, #23356, #84769, #22352, #46213, #53339, #52830, #15757, #8155, #39093, #7651, #69559, #60462, #61950, #1044, #84267, #78141, #91380, #14751, #45719, #70050, #14249, #85264, #31484, #77147, #47219, #8656, #62447, #23862, #54839, #53838, #38, #7143, #39598, #85779, #30484, #16261, #38095, #69048, #99975, #95390, #94385, #71062, #24373, #55844, #33488, #88285, #93885, #16754, #18757, #64974, #2552, #78640, #87271, #18266, #56352, #41115, #26382, #64476, #9656, #25880, #49736, #73068, #79156, #71565, #32998, #80665, #72072, #1551, #3056, #17771, #11151, #63973, #9146, #32491, #24868, #62957, #2058, #42128, #48226, #94883, #56851, #40611, #31988, #87783, #48736, #63464, #49238, #10154, #55342, #86274, #47724, #72562, #40105, #86772, #33998, #25374, #17262, #79656, #80168, #10659, #95887, #41619, #57353, #4554, #27875, #35985, #59837, #73558, #81668, #35500, #82657, #28369, #42621, #12140, #28874, #65971, #34991, #66957, #66475, #58832, #90774, #74550, #57850, #34496, #74056, #52220, #19747, #97390, #12643, #43111, #21246, #5037, #89780, #97871, #20250, #36481, #4049, #51217, #82160, #20748, #96891, #26880, #5530, #43606, #83149, #3552, #59328, #90274, #44104, #44603, #27383, #51716, #13135, #13633, #58345, #75032, #67446, #98371, #65471, #89280, #96388, #88790, #19255, #50226, #81165, #50722, #11645, #45113, #14134, #46104, #61836, #75530, #77032, #76526, #91270, #7031, #76031, #67949, #7533, #38487, #69435, #99860, #30365, #6033, #53723, #92758, #46609, #14641, #54226, #22738, #85151, #21742, #99373, #100354, #30871, #37984, #15641, #77531, #84653, #23242, #8028, #45605, #92262, #6538, #36985, #98876, #15141, #68437, #52715, #61339, #83652, #29366, #60345, #68934, #29869, #37485, #60840, #91757, #84150, #22238, #53222, #98700, #36316, #11974, #20576, #59158, #35324, #75857, #5362, #44434, #52041, #21074, #82479, #6361, #12472, #4867, #66789, #52537, #74858, #4376, #36815, #90102, #21565, #97707, #42942, #73877, #28201, #81988, #83473, #27209, #50540, #13960, #29198, #60167, #89107, #75358, #82970, #51548, #67276, #91089, #98194, #43440, #28704, #44936, #65791, #74371, #35815, #12960, #96706, #59664, #66285, #67782, #43928, #58163, #19580, #13460, #97211, #58653, #81494, #90595, #27707, #5858, #89601, #20081, #51049, #93573, #7848, #61659, #76351, #69758, #15456, #85976, #47421, #30688, #54532, #6853, #60663, #39297, #100171, #24068, #37318, #239, #84971, #77843, #78349, #30182, #38297, #92577, #31181, #55038, #37807, #14956, #69253, #29693, #8349, #46416, #45930, #62658, #99679, #68759, #62155, #23055, #54045, #16451, #38797, #91585, #77348, #61165, #93078, #23563, #53046, #85467, #92084, #31690, #68265, #15952, #737, #99192, #70254, #45436, #46918, #22065, #83976, #14456, #22554, #53546, #84476, #76840, #7342, #80912, #88530, #64214, #4295, #73309, #73797, #42866, #41869, #49985, #79907, #97135, #35245, #26633, #10397, #33234, #96146, #2303, #57593, #11403, #26126, #65715, #95140, #66215, #9896, #87532, #18012, #72813, #57097, #48975, #42377, #25626, #56598, #10906, #65222, #96628, #71813, #27131, #41355, #3804, #3316, #27635, #72309, #88034, #34247, #20007, #2806, #34742, #58580, #33743, #40847, #64724, #95641, #50467, #18508, #19006, #58095, #89031, #19506, #81416, #11897, #89523, #50974, #49482, #80412, #20496, #45354, #90516, #76276, #59586, #83900, #82402, #37725, #43854, #12881, #99113, #6770, #81911, #68186, #60589, #91012, #20994, #60088, #52965, #68685, #29609, #37235, #29113, #21485, #12389, #83396, #14378, #99604, #13380, #30107, #52464, #61080, #97626, #67203, #6277, #13881, #44855, #35745, #92009, #51966, #91505, #43362, #28622, #28130, #82895, #44360, #21984, #75284, #22480, #74298, #5281, #74783, #75778, #36242, #51468, #4790, #98116, #66716, #59087, #90024, #5779, #36734, #67702, #98619, #76765, #63080, #39718, #77764, #62574, #47846, #23992, #31105, #54961, #71185, #94511, #164, #93000, #54456, #40233, #93499, #85900, #46845, #100095, #1675, #78768, #70175, #53965, #7265, #39218, #45846, #660, #16379, #69682, #8780, #38219, #9268, #62076, #31607, #55463, #23475, #86400, #47345, #30609, #8277, #78269, #22975, #63589, #70677, #32107, #1171, #94006, #24494, #46339, #7774, #61584, #16885, #92504, #32613, #15376, #53470, #84399, #14879, #85390, #84895, #77270, #15880, #69175, #38720, #96017, #9775, #48352, #26001, #80291, #11277, #86897, #42258, #40729, #18884, #56973, #57974, #35124, #71687, #65596, #66097, #64094, #57476, #19384, #87400, #55970, #95012, #17389, #96512, #41236, #87909, #41748, #72689, #3679, #49361, #34627, #73189, #18391, #27007, #49865, #25503, #88913, #33619, #50351, #2680, #81290, #56475, #11774, #17895, #48857, #42747, #73680, #24992, #4174, #79281, #34126, #64601, #79782, #2184, #80797, #33116, #10279, #3186, #65098, #72191, #26512, #95515, #10784, #88410, #91387, #67576, #21864, #12263, #82286, #21369, #98493, #75167, #83774, #14256, #59966, #60469, #29485, #28495, #36608, #66598, #20876, #89404, #68070, #5657, #74667, #52838, #58962, #28005, #28995, #59456, #51847, #45232, #13757, #76155, #97014, #83279, #75654, #90896, #5164, #52343, #98994, #6654, #27514, #82780, #37610, #58469, #37108, #4675, #13262, #19876, #43242, #50851, #44730, #81790, #74179, #12762, #6155, #35624, #97510, #89902, #20371, #36115, #51345, #43733, #67084, #97994, #90401, #44236, #46220, #23871, #38606, #85787, #54346, #60960, #85273, #8162, #84775, #54846, #91885, #62966, #15263, #46729, #70558, #69566, #45725, #29988, #1055, #22358, #78149, #16269, #92883, #77655, #47228, #8664, #39606, #15764, #61459, #22857, #14756, #39100, #76648, #31491, #30490, #70057, #61957, #7150, #68562, #53347, #31996, #69056, #92385, #99493, #543, #84274, #38102, #44, #23362, #93893, #99981, #24381, #53844, #62455, #30990, #55350, #77154, #7657, #93383, #86282, #16764, #47732, #78648, #9155, #71071, #9667, #32501, #80674, #56362, #41125, #56861, #87793, #18766, #64485, #49748, #57363, #88295, #24877, #34007, #72081, #73077, #40621, #17781, #33499, #71575, #63473, #42137, #2563, #26889, #40115, #72572, #18277, #11162, #81174, #33007, #95400, #25889, #3067, #96399, #2068, #48745, #49249, #3562, #64983, #80176, #79666, #65480, #63982, #94893, #95897, #10668, #41630, #57861, #26392, #94395, #34507, #25385, #88800, #19265, #55854, #50236, #87280, #1561, #86781, #17273, #48235, #79166, #10165, #19756, #35994, #21751, #58354, #29377, #52725, #50732, #81677, #11653, #59337, #35511, #20757, #66968, #98886, #60354, #75044, #98381, #42630, #58842, #89290, #51227, #89789, #67455, #82171, #28884, #59848, #66486, #12151, #5540, #74069, #43120, #4058, #97399, #13144, #67959, #73568, #12654, #4563, #35002, #44613, #65982, #21255, #90785, #97880, #51729, #6043, #82666, #20259, #44116, #91280, #96900, #43618, #74559, #5047, #27394, #36490, #52229, #28378, #27885, #90286, #83159, #13643, #75539, #36994, #14144, #53732, #31885, #99869, #84663, #92767, #61348, #39498, #54235, #7542, #23253, #38497, #78033, #92272, #23757, #69939, #83662, #30376, #29878, #22749, #15150, #38989, #46114, #427, #31380, #7042, #84159, #46619, #45615, #22249, #76041, #37994, #77041, #61846, #85668, #69446, #60849, #45122, #16149, #6548, #93269, #62343, #100364, #85161, #8545, #15650, #30880, #77540, #935, #24266, #8039, #54734, #91767, #47120, #76535, #70448, #62858, #53231, #37495, #68447, #93775, #14650, #68944, #99383, #25263, #3451, #71457, #56242, #64362, #32889, #11048, #25769, #39994, #49127, #87167, #88177, #55738, #63861, #48627, #72454, #24757, #78537, #57242, #17656, #42012, #55240, #87673, #2440, #95780, #96282, #48119, #79552, #33883, #10042, #64867, #2948, #26270, #41002, #47618, #18645, #95284, #94775, #80553, #17153, #86664, #18154, #71959, #33374, #72955, #56741, #9041, #80054, #41501, #49623, #10540, #34386, #65363, #86166, #16648, #70955, #1443, #32381, #63357, #94274, #79048, #9542, #40503, #1945, #44495, #67841, #65859, #96777, #12036, #51607, #5423, #51108, #36375, #43987, #74919, #82052, #19148, #98256, #35878, #4442, #52107, #89171, #58232, #59219, #58717, #12533, #13523, #97769, #90657, #26769, #13023, #67335, #66847, #35392, #4931, #28764, #21136, #57734, #43501, #83033, #75418, #59727, #34883, #74438, #36875, #73450, #5920, #88676, #50116, #42512, #43003, #82543, #28263, #90165, #81055, #11537, #66354, #3943, #27276, #19644, #73945, #50608, #97279, #27767, #81561, #89668, #20145, #20639, #99260, #61724, #60726, #37380, #91153, #22128, #100239, #54600, #60228, #83537, #85535, #31250, #69318, #45000, #53613, #92147, #68326, #8418, #38365, #77411, #76415, #30753, #16019, #39369, #45499, #37872, #99742, #46987, #7409, #29759, #69822, #22622, #77910, #30247, #75920, #6426, #61228, #14524, #91647, #92644, #6918, #68825, #23123, #84538, #98761, #54112, #15022, #53111, #85033, #76911, #29254, #21628, #14019, #38864, #52601, #84042, #15519, #93141, #45992, #46483, #7916, #306, #62221, #23625, #63223, #71329, #94653, #41378, #64745, #805, #25132, #33762, #18528, #10416, #78419, #56112, #80433, #16517, #88053, #10924, #95662, #86040, #55611, #95159, #40870, #48498, #24137, #26143, #47991, #72330, #56618, #70324, #17027, #47487, #9411, #78918, #25643, #40374, #87547, #18029, #62725, #87040, #9916, #86540, #48996, #93641, #57116, #1816, #79422, #2823, #32753, #8916, #31757, #49500, #55104, #79925, #39866, #17531, #71830, #70825, #1315, #32253, #2323, #94145, #24631, #63736, #33252, #64234, #6172, #3823, #50996, #35270, #88552, #41888, #65242, #60484, #42397, #34761, #72835, #11919, #26652, #96163, #42884, #97161, #29502, #3334, #91401, #57613, #37123, #73816, #76171, #73330, #19524, #66235, #21878, #11422, #19027, #45246, #4318, #30003, #65734, #34270, #83792, #58116, #27655, #58600, #89547, #52854, #20031, #14272, #6670, #37622, #81931, #50002, #68580, #13771, #50488, #99505, #96652, #27151, #89053, #60975, #81438, #44748, #91900, #22377, #80935, #53362, #84289, #75670, #68084, #99007, #77669, #31007, #92400, #85804, #99996, #38116, #15780, #70073, #71086, #16284, #39119, #53859, #47244, #93399, #63491, #24893, #30505, #55366, #55873, #84793, #78169, #9173, #77169, #45739, #15276, #7167, #86297, #61973, #7674, #46746, #561, #8682, #1579, #46238, #92900, #8178, #93907, #39622, #38621, #78664, #23378, #40132, #54361, #16785, #69581, #32516, #64, #85293, #69072, #23891, #31508, #70576, #62471, #61476, #54863, #1071, #76662, #32012, #62986, #24398, #47749, #94410, #14773, #22873, #57876, #73584, #18294, #81190, #25402, #56377, #27408, #34021, #10180, #95915, #10682, #4072, #35022, #49762, #50251, #19279, #49265, #26407, #87298, #65996, #11668, #3084, #17796, #9680, #41143, #48759, #80689, #79685, #72095, #79183, #2576, #88310, #42649, #48252, #71590, #96914, #86796, #57382, #33022, #41644, #80193, #33517, #17288, #18781, #73091, #42152, #64999, #64501, #95416, #63997, #11181, #94910, #3581, #25904, #34523, #72590, #56878, #40639, #2084, #65496, #96417, #26903, #87808, #88813, #68465, #4577, #76062, #99400, #97412, #27900, #58367, #5558, #82182, #67469, #82680, #45136, #6563, #21270, #21765, #91296, #90299, #98395, #58856, #37510, #13656, #28391, #75555, #44629, #12668, #89802, #52246, #20272, #51240, #50748, #43632, #59865, #14160, #19774, #43134, #89306, #52739, #28898, #35527, #13161, #6057, #44132, #90800, #75057, #81694, #37011, #36505, #74571, #5061, #66498, #83172, #36008, #67976, #66983, #98899, #51747, #97896, #12166, #74085, #29394, #20768, #59351, #60373, #83678, #14666, #53247, #30896, #85180, #16166, #91783, #47134, #45631, #23776, #61863, #62875, #30391, #7559, #23267, #78051, #99883, #62358, #24287, #92292, #60863, #61364, #22264, #70465, #46131, #92785, #46636, #77554, #8565, #54251, #39514, #951, #31900, #15667, #84176, #93791, #39006, #38510, #55254, #69459, #86183, #22764, #16666, #53749, #84678, #47637, #78553, #29895, #9058, #40009, #69959, #100382, #8057, #70969, #76550, #7058, #444, #38010, #31397, #68960, #77057, #93284, #54751, #85686, #15164, #72470, #25783, #40524, #33897, #80072, #50130, #11550, #86682, #42028, #42528, #71474, #64883, #64380, #88691, #1460, #95793, #49145, #72972, #32400, #94791, #2456, #56759, #26286, #57750, #1963, #79570, #33390, #80567, #57262, #32905, #65377, #10060, #63876, #25280, #88192, #95299, #87688, #19160, #2965, #55755, #10557, #56258, #18662, #18173, #17169, #41516, #87183, #63375, #49637, #11062, #3464, #34400, #96298, #9556, #26785, #94289, #48135, #81074, #24773, #17671, #48644, #79064, #41021, #71975, #82559, #97784, #60244, #91171, #36390, #36888, #5934, #4945, #19658, #12550, #51122, #28778, #43516, #90675, #59741, #97293, #73961, #67353, #35409, #12048, #65874, #27780, #74933, #29274, #34901, #58244, #21642, #67854, #98775, #96793, #83046, #21152, #58734, #66366, #52615, #3956, #82066, #5438, #83554, #14036, #20158, #74453, #35891, #73463, #13041, #43018, #44508, #28276, #27289, #89188, #52122, #4457, #89682, #13536, #50623, #81575, #75434, #66861, #44000, #59235, #51625, #90179, #20653, #98273, #69334, #8437, #93661, #85553, #46502, #16036, #31776, #76927, #39386, #15537, #70341, #60740, #30264, #69843, #77428, #23140, #99277, #823, #22639, #47003, #31269, #45016, #92165, #91664, #53631, #322, #15039, #62238, #93157, #68841, #45515, #7931, #6936, #84057, #37396, #99759, #38881, #62747, #6441, #29775, #24155, #77926, #23648, #22144, #54618, #55123, #61243, #37888, #86059, #75937, #84553, #68344, #53129, #14541, #46010, #7428, #38382, #76430, #54128, #100254, #30773, #61743, #92661, #85052, #33779, #17044, #9429, #47509, #87060, #65259, #32772, #17549, #25662, #94670, #72850, #87564, #40889, #55630, #49014, #95178, #96184, #26670, #1336, #57136, #86561, #39885, #18548, #79444, #3352, #16533, #79948, #64256, #88071, #57629, #40394, #48515, #71849, #10433, #34287, #48012, #25153, #9935, #95679, #41394, #56634, #56132, #41909, #78936, #71346, #72350, #2339, #33268, #78435, #18050, #2846, #64763, #8935, #26162, #49517, #1836, #63754, #63242, #80451, #94164, #10944, #70844, #32270, #24648, #44396, #89564, #65750, #96671, #51011, #4336, #27170, #59126, #73347, #11438, #20049, #43399, #74824, #50019, #5318, #3840, #20534, #66752, #36776, #98655, #34782, #28661, #29154, #58131, #51508, #82933, #50504, #19045, #89068, #80954, #59622, #35288, #81945, #4828, #35782, #67240, #75323, #19544, #66251, #12431, #98154, #12922, #81460, #52004, #97176, #13421, #27671, #90555, #11936, #5817, #42901, #73837, #36282, #67740, #88570, #21033, #74337, #58620, #97669, #28167, #42417, #43891, #90061, #82440, #7305, #69215, #60127, #61625, #31148, #46884, #92049, #54492, #30654, #85430, #75820, #45395, #83940, #100131, #84436, #77802, #8315, #23016, #23517, #93038, #22519, #92544, #29653, #39259, #15916, #76804, #60627, #83433, #45889, #52503, #38256, #54004, #99153, #13921, #14420, #84934, #70219, #21526, #44898, #699, #91053, #15417, #6319, #14915, #53513, #91548, #46377, #37767, #61118, #38756, #77311, #22021, #68724, #37274, #53010, #76311, #7812, #69725, #203, #68226, #62117, #6811, #99642, #30144, #95050, #56008, #47386, #86933, #32144, #93535, #87436, #79817, #95552, #80325, #72224, #39756, #17425, #41784, #78313, #49397, #72725, #70715, #1212, #31645, #79319, #55501, #40764, #48384, #18427, #10815, #25541, #26034, #62614, #78804, #8819, #71222, #9302, #17931, #1712, #48890, #10314, #86439, #63121, #56509, #94045, #24531, #24031, #16924, #33147 ),
 .UNSPECIFIED., .F., .F.,
 ( 4, 2, 2, 2, 2, 2, 2, 2, 2, 2, 2, 2, 2, 2, 2, 2, 2, 2, 2, 2, 2, 2, 2, 2, 2, 2, 2, 2, 2, 2, 2, 2, 2, 2, 2, 2, 2, 2, 2, 2, 2, 2, 2, 2, 2, 2, 2, 2, 2, 2, 2, 2, 2, 2, 2, 2, 2, 2, 2, 2, 2, 2, 2, 2, 2, 2, 2, 2, 2, 2, 2, 2, 2, 2, 2, 2, 2, 2, 2, 2, 2, 2, 2, 2, 2, 2, 2, 2, 2, 2, 2, 2, 2, 2, 2, 2, 2, 2, 2, 2, 2, 2, 2, 2, 2, 2, 2, 2, 2, 2, 2, 2, 2, 2, 2, 2, 2, 2, 2, 2, 2, 2, 2, 2, 2, 2, 2, 2, 2, 2, 2, 2, 2, 2, 2, 2, 2, 2, 2, 2, 2, 2, 2, 2, 2, 2, 2, 2, 2, 2, 2, 2, 2, 2, 2, 2, 2, 2, 2, 2, 2, 2, 2, 2, 2, 2, 2, 2, 2, 2, 2, 2, 2, 2, 2, 2, 2, 2, 2, 2, 2, 2, 2, 2, 2, 2, 2, 2, 2, 2, 2, 2, 2, 2, 2, 2, 2, 2, 2, 2, 2, 2, 2, 2, 2, 2, 2, 2, 2, 2, 2, 2, 2, 2, 2, 2, 2, 2, 2, 2, 2, 2, 2, 2, 2, 2, 2, 2, 2, 2, 2, 2, 2, 2, 2, 2, 2, 2, 2, 2, 2, 2, 2, 2, 2, 2, 2, 2, 2, 2, 2, 2, 2, 2, 2, 2, 2, 2, 2, 2, 2, 2, 2, 2, 2, 2, 2, 2, 2, 2, 2, 2, 2, 2, 2, 2, 2, 2, 2, 2, 2, 2, 2, 2, 2, 2, 2, 2, 2, 2, 2, 2, 2, 2, 2, 2, 2, 2, 2, 2, 2, 2, 2, 2, 2, 2, 2, 2, 2, 2, 2, 2, 2, 2, 2, 2, 2, 2, 2, 2, 2, 2, 2, 2, 2, 2, 2, 2, 2, 2, 2, 2, 2, 2, 2, 2, 2, 2, 2, 2, 2, 2, 2, 2, 2, 2, 2, 2, 2, 2, 2, 2, 2, 2, 2, 2, 2, 2, 2, 2, 2, 2, 2, 2, 2, 2, 2, 2, 2, 2, 2, 2, 2, 2, 2, 2, 2, 2, 2, 2, 2, 2, 2, 2, 2, 2, 2, 2, 2, 2, 2, 2, 2, 2, 2, 2, 2, 2, 2, 2, 2, 2, 2, 2, 2, 2, 2, 2, 2, 2, 2, 2, 2, 2, 2, 2, 2, 2, 2, 2, 2, 2, 2, 2, 2, 2, 2, 2, 2, 2, 2, 2, 2, 2, 2, 2, 2, 2, 2, 2, 2, 2, 2, 2, 2, 2, 2, 2, 2, 2, 2, 2, 2, 2, 2, 2, 2, 2, 2, 2, 2, 2, 2, 2, 2, 2, 2, 2, 2, 2, 2, 2, 2, 2, 2, 2, 2, 2, 2, 2, 2, 2, 2, 2, 2, 2, 2, 2, 2, 2, 2, 2, 2, 2, 2, 2, 2, 2, 2, 2, 2, 2, 2, 2, 2, 2, 2, 2, 2, 2, 2, 2, 2, 2, 2, 2, 2, 2, 2, 2, 2, 2, 2, 2, 2, 2, 2, 2, 2, 2, 2, 2, 2, 2, 2, 2, 2, 2, 2, 2, 2, 2, 2, 2, 2, 2, 2, 2, 2, 2, 2, 2, 2, 2, 2, 2, 2, 2, 2, 2, 2, 2, 2, 2, 2, 2, 2, 2, 2, 2, 2, 2, 2, 2, 2, 2, 2, 2, 2, 2, 2, 2, 2, 2, 2, 2, 2, 2, 2, 2, 2, 2, 2, 2, 2, 2, 2, 2, 2, 2, 2, 2, 2, 2, 2, 2, 2, 2, 2, 2, 2, 2, 2, 2, 2, 2, 2, 2, 2, 2, 2, 2, 2, 2, 2, 2, 2, 2, 2, 2, 2, 2, 2, 2, 2, 2, 2, 2, 2, 2, 2, 2, 2, 2, 2, 2, 2, 2, 2, 2, 2, 2, 2, 2, 2, 2, 2, 2, 2, 2, 2, 2, 2, 2, 2, 2, 2, 2, 2, 2, 2, 2, 2, 2, 2, 2, 2, 2, 2, 2, 2, 2, 2, 2, 2, 2, 2, 2, 2, 2, 2, 2, 2, 2, 2, 2, 2, 2, 2, 2, 2, 2, 2, 2, 2, 2, 2, 2, 2, 2, 2, 2, 2, 2, 2, 2, 2, 2, 2, 2, 2, 2, 2, 2, 2, 2, 2, 2, 2, 2, 2, 2, 2, 2, 2, 2, 2, 2, 2, 2, 2, 2, 2, 2, 2, 2, 2, 2, 2, 2, 2, 2, 2, 2, 2, 2, 2, 2, 2, 2, 2, 2, 2, 2, 2, 2, 2, 2, 2, 2, 2, 2, 2, 2, 2, 2, 2, 2, 2, 2, 2, 2, 2, 2, 2, 2, 2, 2, 2, 2, 2, 2, 2, 2, 2, 2, 2, 2, 2, 2, 2, 2, 2, 2, 2, 2, 2, 2, 2, 2, 2, 2, 2, 2, 2, 2, 2, 2, 2, 2, 2, 2, 2, 2, 2, 2, 2, 2, 2, 2, 2, 2, 2, 2, 2, 2, 2, 2, 2, 2, 2, 2, 2, 2, 2, 2, 2, 2, 2, 2, 2, 2, 2, 2, 2, 2, 2, 2, 2, 2, 2, 2, 2, 2, 2, 2, 2, 2, 2, 2, 2, 2, 2, 2, 2, 2, 2, 2, 2, 2, 2, 2, 2, 2, 2, 2, 2, 2, 2, 2, 2, 2, 2, 2, 2, 2, 2, 2, 2, 2, 2, 2, 2, 2, 2, 2, 2, 2, 2, 2, 2, 2, 2, 2, 2, 2, 2, 2, 2, 2, 2, 2, 2, 2, 2, 2, 2, 2, 2, 2, 2, 2, 2, 2, 2, 2, 2, 2, 2, 2, 2, 2, 2, 2, 2, 2, 2, 2, 2, 2, 2, 2, 2, 2, 2, 2, 2, 2, 2, 2, 2, 2, 2, 2, 2, 2, 2, 2, 2, 2, 2, 2, 2, 2, 2, 2, 2, 2, 2, 2, 2, 2, 2, 2, 2, 2, 2, 2, 2, 2, 2, 2, 2, 2, 2, 2, 2, 2, 2, 2, 2, 2, 2, 2, 2, 2, 2, 2, 2, 2, 2, 2, 2, 2, 2, 2, 2, 2, 2, 2, 2, 2, 2, 2, 2, 2, 2, 2, 2, 2, 2, 2, 2, 2, 2, 2, 2, 2, 2, 2, 2, 2, 2, 2, 2, 2, 2, 2, 2, 2, 2, 2, 2, 2, 2, 2, 2, 2, 2, 2, 2, 2, 2, 2, 2, 2, 2, 2, 2, 2, 2, 2, 2, 2, 2, 2, 2, 2, 2, 2, 2, 2, 2, 2, 2, 2, 2, 2, 2, 2, 2, 2, 2, 2, 2, 2, 2, 2, 2, 2, 2, 2, 2, 2, 2, 2, 2, 2, 2, 2, 2, 2, 2, 2, 2, 2, 2, 2, 2, 2, 2, 2, 2, 2, 2, 2, 2, 2, 2, 2, 2, 2, 2, 2, 2, 2, 2, 2, 2, 2, 2, 2, 2, 2, 2, 2, 2, 2, 2, 2, 2, 2, 2, 2, 2, 2, 2, 2, 2, 2, 2, 2, 2, 2, 2, 2, 2, 2, 2, 2, 2, 2, 2, 2, 2, 2, 2, 2, 2, 2, 2, 2, 2, 2, 2, 2, 2, 2, 2, 2, 2, 2, 2, 2, 2, 2, 2, 2, 2, 2, 2, 2, 2, 2, 2, 2, 2, 2, 2, 2, 2, 2, 2, 2, 2, 2, 2, 2, 2, 2, 2, 2, 2, 2, 2, 2, 2, 2, 2, 2, 2, 2, 2, 2, 2, 2, 2, 2, 2, 2, 2, 2, 2, 2, 2, 2, 2, 2, 2, 2, 2, 2, 2, 2, 2, 2, 2, 2, 2, 2, 2, 2, 2, 2, 2, 2, 2, 2, 2, 2, 2, 2, 2, 2, 2, 2, 2, 2, 2, 2, 2, 2, 2, 2, 2, 2, 2, 2, 2, 2, 2, 2, 2, 2, 2, 2, 2, 2, 2, 2, 2, 2, 2, 2, 2, 2, 2, 2, 2, 2, 2, 2, 2, 2, 2, 2, 2, 2, 2, 2, 2, 2, 2, 2, 2, 2, 2, 2, 2, 2, 2, 2, 2, 2, 2, 2, 2, 2, 2, 2, 2, 2, 2, 2, 2, 2, 2, 2, 2, 2, 2, 2, 2, 2, 2, 2, 2, 2, 2, 2, 2, 2, 2, 2, 2, 2, 2, 2, 2, 2, 2, 2, 2, 2, 2, 2, 2, 2, 2, 2, 2, 2, 2, 2, 2, 2, 2, 2, 2, 2, 2, 2, 2, 2, 2, 2, 2, 2, 2, 2, 2, 2, 2, 2, 2, 2, 2, 2, 2, 2, 2, 2, 2, 2, 2, 2, 2, 2, 2, 2, 2, 2, 2, 2, 2, 2, 2, 2, 2, 2, 2, 2, 2, 2, 2, 2, 2, 2, 2, 2, 2, 2, 2, 2, 2, 2, 2, 2, 2, 2, 2, 2, 2, 2, 2, 2, 2, 2, 2, 2, 2, 2, 2, 2, 2, 2, 2, 2, 2, 2, 2, 2, 2, 2, 2, 2, 2, 2, 2, 2, 2, 2, 2, 2, 2, 2, 2, 2, 2, 2, 2, 2, 2, 2, 2, 2, 2, 2, 2, 2, 2, 2, 2, 2, 2, 2, 2, 2, 2, 2, 2, 2, 2, 2, 2, 2, 2, 2, 2, 2, 2, 2, 2, 2, 2, 2, 2, 2, 2, 2, 2, 2, 2, 2, 2, 2, 2, 2, 2, 2, 2, 2, 2, 2, 2, 2, 2, 2, 2, 2, 2, 2, 2, 2, 2, 2, 2, 2, 2, 2, 2, 2, 2, 2, 2, 2, 2, 2, 2, 2, 2, 2, 2, 2, 2, 2, 2, 2, 2, 2, 2, 2, 2, 2, 2, 2, 2, 2, 2, 2, 2, 2, 2, 2, 2, 2, 2, 2, 2, 2, 2, 2, 2, 2, 2, 2, 2, 2, 2, 2, 2, 2, 2, 2, 2, 2, 2, 2, 2, 2, 2, 2, 2, 2, 2, 2, 2, 2, 2, 2, 2, 2, 2, 2, 2, 2, 2, 2, 2, 2, 2, 2, 2, 2, 2, 2, 2, 2, 2, 2, 2, 2, 2, 2, 2, 2, 2, 2, 2, 2, 2, 2, 2, 2, 2, 2, 2, 2, 2, 2, 2, 2, 2, 2, 2, 2, 2, 2, 2, 2, 2, 2, 2, 2, 2, 2, 2, 2, 2, 2, 2, 2, 2, 2, 2, 2, 2, 2, 2, 2, 2, 2, 2, 2, 2, 2, 2, 2, 2, 2, 2, 2, 2, 2, 2, 2, 2, 2, 2, 2, 2, 2, 2, 2, 2, 2, 2, 2, 2, 2, 2, 2, 2, 2, 2, 2, 2, 2, 2, 2, 2, 2, 2, 2, 2, 2, 2, 2, 2, 2, 2, 2, 2, 2, 2, 2, 2, 2, 2, 2, 2, 2, 2, 2, 2, 2, 2, 2, 2, 2, 2, 2, 2, 2, 2, 2, 2, 2, 2, 2, 2, 2, 2, 2, 2, 2, 2, 2, 2, 2, 2, 2, 2, 2, 2, 2, 2, 2, 2, 2, 2, 2, 2, 2, 2, 2, 2, 2, 2, 2, 2, 2, 2, 2, 2, 2, 2, 2, 2, 2, 2, 2, 2, 2, 2, 2, 2, 2, 2, 2, 2, 2, 2, 2, 2, 2, 2, 2, 2, 2, 2, 2, 2, 2, 2, 2, 2, 2, 2, 2, 2, 2, 2, 2, 2, 2, 2, 2, 2, 2, 2, 2, 2, 2, 2, 2, 2, 2, 2, 2, 2, 2, 2, 2, 2, 2, 2, 2, 2, 2, 2, 2, 2, 2, 2, 2, 2, 2, 2, 2, 2, 2, 2, 2, 2, 2, 2, 2, 2, 2, 2, 2, 2, 2, 2, 2, 2, 2, 2, 2, 2, 2, 2, 2, 2, 2, 2, 2, 2, 2, 2, 2, 2, 2, 2, 2, 2, 2, 2, 2, 2, 2, 2, 2, 2, 2, 2, 2, 2, 2, 2, 2, 2, 2, 2, 2, 2, 2, 2, 2, 2, 2, 2, 2, 2, 2, 2, 2, 2, 2, 2, 2, 2, 2, 2, 2, 2, 2, 2, 2, 2, 2, 2, 2, 2, 2, 2, 2, 2, 2, 2, 2, 2, 2, 2, 2, 2, 2, 2, 2, 2, 2, 2, 2, 2, 2, 2, 2, 2, 2, 2, 2, 2, 2, 2, 2, 2, 2, 2, 2, 2, 2, 2, 2, 2, 2, 2, 2, 2, 2, 2, 2, 2, 2, 2, 2, 2, 2, 2, 2, 2, 2, 2, 2, 2, 2, 2, 2, 2, 2, 2, 2, 2, 2, 2, 2, 2, 2, 4 ),
 ( 0.000000000000000000, 0.0004882812500000001084, 0.0009765625000000002168, 0.001464843750000000434, 0.001953125000000000000, 0.002441406250000000000, 0.002929687499999999566, 0.003417968749999999566, 0.003906249999999999133, 0.004394531249999998265, 0.004882812499999997398, 0.005371093749999997398, 0.005859374999999997398, 0.006347656249999998265, 0.006835937499999998265, 0.007324218749999998265, 0.007812499999999998265, 0.008300781249999998265, 0.008789062499999998265, 0.009277343749999998265, 0.009765624999999998265, 0.01025390624999999827, 0.01074218749999999827, 0.01123046874999999827, 0.01171874999999999827, 0.01220703125000000000, 0.01269531250000000000, 0.01318359375000000000, 0.01367187500000000000, 0.01416015625000000000, 0.01464843750000000000, 0.01513671875000000000, 0.01562500000000000000, 0.01611328125000000000, 0.01660156250000000000, 0.01708984375000000000, 0.01757812500000000000, 0.01806640625000000000, 0.01855468750000000000, 0.01904296875000000000, 0.01953125000000000000, 0.02001953125000000000, 0.02050781250000000000, 0.02099609375000000000, 0.02148437500000000000, 0.02197265625000000000, 0.02246093750000000000, 0.02294921875000000000, 0.02343750000000000000, 0.02392578125000000347, 0.02441406250000000347, 0.02490234375000000347, 0.02539062500000000347, 0.02587890625000000347, 0.02636718750000000347, 0.02685546875000000347, 0.02734375000000000347, 0.02783203125000000347, 0.02832031250000000347, 0.02880859375000000347, 0.02929687500000000347, 0.02978515625000000347, 0.03027343750000000347, 0.03076171875000000347, 0.03125000000000000000, 0.03173828125000000000, 0.03222656250000000000, 0.03271484375000000000, 0.03320312500000000000, 0.03369140625000000000, 0.03417968750000000000, 0.03466796875000000000, 0.03515625000000000000, 0.03564453125000000000, 0.03613281250000000000, 0.03662109375000000000, 0.03710937500000000000, 0.03759765625000000000, 0.03808593750000000000, 0.03857421875000000000, 0.03906250000000000000, 0.03955078125000000000, 0.04003906250000000000, 0.04052734375000000000, 0.04101562500000000000, 0.04150390625000000000, 0.04199218750000000000, 0.04248046875000000000, 0.04296875000000000000, 0.04345703125000000000, 0.04394531250000000000, 0.04443359375000000000, 0.04492187500000000000, 0.04541015625000000000, 0.04589843750000000000, 0.04638671875000000000, 0.04687500000000000000, 0.04736328125000000694, 0.04785156250000000694, 0.04833984375000000694, 0.04882812500000000694, 0.04931640625000000694, 0.04980468750000000694, 0.05029296875000000694, 0.05078125000000000694, 0.05126953125000000694, 0.05175781250000000694, 0.05224609375000000694, 0.05273437500000000694, 0.05322265625000000694, 0.05371093750000000694, 0.05419921875000000694, 0.05468750000000000694, 0.05517578125000000694, 0.05566406250000000694, 0.05615234375000000694, 0.05664062500000000694, 0.05712890625000000694, 0.05761718750000000694, 0.05810546875000000694, 0.05859375000000000694, 0.05908203125000000694, 0.05957031250000000694, 0.06005859375000000694, 0.06054687500000000694, 0.06103515625000000694, 0.06152343750000000694, 0.06201171875000000694, 0.06250000000000000000, 0.06298828125000000000, 0.06347656250000000000, 0.06396484375000000000, 0.06445312500000000000, 0.06494140625000000000, 0.06542968750000000000, 0.06591796875000000000, 0.06640625000000000000, 0.06689453125000000000, 0.06738281250000000000, 0.06787109375000000000, 0.06835937500000000000, 0.06884765625000000000, 0.06933593750000000000, 0.06982421875000000000, 0.07031250000000000000, 0.07080078125000000000, 0.07128906250000000000, 0.07177734375000000000, 0.07226562500000000000, 0.07275390625000000000, 0.07324218750000000000, 0.07373046875000000000, 0.07421875000000000000, 0.07470703125000000000, 0.07519531250000000000, 0.07568359375000000000, 0.07617187500000000000, 0.07666015625000000000, 0.07714843750000000000, 0.07763671875000000000, 0.07812500000000000000, 0.07861328125000000000, 0.07910156250000000000, 0.07958984375000000000, 0.08007812500000000000, 0.08056640625000000000, 0.08105468750000000000, 0.08154296875000000000, 0.08203125000000000000, 0.08251953125000000000, 0.08300781250000000000, 0.08349609375000000000, 0.08398437500000000000, 0.08447265625000000000, 0.08496093750000000000, 0.08544921875000000000, 0.08593750000000000000, 0.08642578125000000000, 0.08691406250000000000, 0.08740234375000000000, 0.08789062500000000000, 0.08837890625000000000, 0.08886718750000000000, 0.08935546875000000000, 0.08984375000000000000, 0.09033203125000000000, 0.09082031250000000000, 0.09130859375000000000, 0.09179687500000000000, 0.09228515625000000000, 0.09277343750000000000, 0.09326171875000000000, 0.09375000000000000000, 0.09423828125000001388, 0.09472656250000001388, 0.09521484375000001388, 0.09570312500000001388, 0.09619140625000001388, 0.09667968750000001388, 0.09716796875000001388, 0.09765625000000001388, 0.09814453125000001388, 0.09863281250000001388, 0.09912109375000001388, 0.09960937500000001388, 0.1000976562500000139, 0.1005859375000000139, 0.1010742187500000139, 0.1015625000000000139, 0.1020507812500000139, 0.1025390625000000139, 0.1030273437500000139, 0.1035156250000000139, 0.1040039062500000139, 0.1044921875000000139, 0.1049804687500000139, 0.1054687500000000139, 0.1059570312500000139, 0.1064453125000000139, 0.1069335937500000139, 0.1074218750000000139, 0.1079101562500000139, 0.1083984375000000139, 0.1088867187500000139, 0.1093750000000000139, 0.1098632812500000139, 0.1103515625000000139, 0.1108398437500000139, 0.1113281250000000139, 0.1118164062500000139, 0.1123046875000000139, 0.1127929687500000139, 0.1132812500000000139, 0.1137695312500000139, 0.1142578125000000139, 0.1147460937500000139, 0.1152343750000000139, 0.1157226562500000139, 0.1162109375000000139, 0.1166992187500000139, 0.1171875000000000139, 0.1176757812500000139, 0.1181640625000000139, 0.1186523437500000139, 0.1191406250000000139, 0.1196289062500000139, 0.1201171875000000139, 0.1206054687500000139, 0.1210937500000000139, 0.1215820312500000139, 0.1220703125000000139, 0.1225585937500000139, 0.1230468750000000139, 0.1235351562500000139, 0.1240234375000000139, 0.1245117187500000139, 0.1250000000000000000, 0.1254882812500000000, 0.1259765625000000000, 0.1264648437500000000, 0.1269531250000000000, 0.1274414062500000000, 0.1279296875000000000, 0.1284179687500000000, 0.1289062500000000000, 0.1293945312500000000, 0.1298828125000000000, 0.1303710937500000000, 0.1308593750000000000, 0.1313476562500000000, 0.1318359375000000000, 0.1323242187500000000, 0.1328125000000000000, 0.1333007812500000000, 0.1337890625000000000, 0.1342773437500000000, 0.1347656250000000000, 0.1352539062500000000, 0.1357421875000000000, 0.1362304687500000000, 0.1367187500000000000, 0.1372070312500000000, 0.1376953125000000000, 0.1381835937500000000, 0.1386718750000000000, 0.1391601562500000000, 0.1396484375000000000, 0.1401367187500000000, 0.1406250000000000000, 0.1411132812500000000, 0.1416015625000000000, 0.1420898437500000000, 0.1425781250000000000, 0.1430664062500000000, 0.1435546875000000000, 0.1440429687500000000, 0.1445312500000000000, 0.1450195312500000000, 0.1455078125000000000, 0.1459960937500000000, 0.1464843750000000000, 0.1469726562500000000, 0.1474609375000000000, 0.1479492187500000000, 0.1484375000000000000, 0.1489257812500000000, 0.1494140625000000000, 0.1499023437500000000, 0.1503906250000000000, 0.1508789062500000000, 0.1513671875000000000, 0.1518554687500000000, 0.1523437500000000000, 0.1528320312500000000, 0.1533203125000000000, 0.1538085937500000000, 0.1542968750000000000, 0.1547851562500000000, 0.1552734375000000000, 0.1557617187500000000, 0.1562500000000000000, 0.1567382812500000000, 0.1572265625000000000, 0.1577148437500000000, 0.1582031250000000000, 0.1586914062500000000, 0.1591796875000000000, 0.1596679687500000000, 0.1601562500000000000, 0.1606445312500000000, 0.1611328125000000000, 0.1616210937500000000, 0.1621093750000000000, 0.1625976562500000000, 0.1630859375000000000, 0.1635742187500000000, 0.1640625000000000000, 0.1645507812500000000, 0.1650390625000000000, 0.1655273437500000000, 0.1660156250000000000, 0.1665039062500000000, 0.1669921875000000000, 0.1674804687500000000, 0.1679687500000000000, 0.1684570312500000000, 0.1689453125000000000, 0.1694335937500000000, 0.1699218750000000000, 0.1704101562500000000, 0.1708984375000000000, 0.1713867187500000000, 0.1718750000000000000, 0.1723632812500000000, 0.1728515625000000000, 0.1733398437500000000, 0.1738281250000000000, 0.1743164062500000000, 0.1748046875000000000, 0.1752929687500000000, 0.1757812500000000000, 0.1762695312500000000, 0.1767578125000000000, 0.1772460937500000000, 0.1777343750000000000, 0.1782226562500000000, 0.1787109375000000000, 0.1791992187500000000, 0.1796875000000000000, 0.1801757812500000000, 0.1806640625000000000, 0.1811523437500000000, 0.1816406250000000000, 0.1821289062500000000, 0.1826171875000000000, 0.1831054687500000000, 0.1835937500000000000, 0.1840820312500000000, 0.1845703125000000000, 0.1850585937500000000, 0.1855468750000000000, 0.1860351562500000000, 0.1865234375000000000, 0.1870117187500000000, 0.1875000000000000000, 0.1879882812500000278, 0.1884765625000000278, 0.1889648437500000278, 0.1894531250000000278, 0.1899414062500000278, 0.1904296875000000278, 0.1909179687500000278, 0.1914062500000000278, 0.1918945312500000278, 0.1923828125000000278, 0.1928710937500000278, 0.1933593750000000278, 0.1938476562500000278, 0.1943359375000000278, 0.1948242187500000278, 0.1953125000000000278, 0.1958007812500000278, 0.1962890625000000278, 0.1967773437500000278, 0.1972656250000000278, 0.1977539062500000278, 0.1982421875000000278, 0.1987304687500000278, 0.1992187500000000278, 0.1997070312500000278, 0.2001953125000000278, 0.2006835937500000278, 0.2011718750000000278, 0.2016601562500000278, 0.2021484375000000278, 0.2026367187500000278, 0.2031250000000000278, 0.2036132812500000278, 0.2041015625000000278, 0.2045898437500000278, 0.2050781250000000278, 0.2055664062500000278, 0.2060546875000000278, 0.2065429687500000278, 0.2070312500000000278, 0.2075195312500000278, 0.2080078125000000278, 0.2084960937500000278, 0.2089843750000000278, 0.2094726562500000278, 0.2099609375000000278, 0.2104492187500000278, 0.2109375000000000278, 0.2114257812500000278, 0.2119140625000000278, 0.2124023437500000278, 0.2128906250000000278, 0.2133789062500000278, 0.2138671875000000278, 0.2143554687500000278, 0.2148437500000000278, 0.2153320312500000278, 0.2158203125000000278, 0.2163085937500000278, 0.2167968750000000278, 0.2172851562500000278, 0.2177734375000000278, 0.2182617187500000278, 0.2187500000000000278, 0.2192382812500000278, 0.2197265625000000278, 0.2202148437500000278, 0.2207031250000000278, 0.2211914062500000278, 0.2216796875000000278, 0.2221679687500000278, 0.2226562500000000278, 0.2231445312500000278, 0.2236328125000000278, 0.2241210937500000278, 0.2246093750000000278, 0.2250976562500000278, 0.2255859375000000278, 0.2260742187500000278, 0.2265625000000000278, 0.2270507812500000278, 0.2275390625000000278, 0.2280273437500000278, 0.2285156250000000278, 0.2290039062500000278, 0.2294921875000000278, 0.2299804687500000278, 0.2304687500000000278, 0.2309570312500000278, 0.2314453125000000278, 0.2319335937500000278, 0.2324218750000000278, 0.2329101562500000278, 0.2333984375000000278, 0.2338867187500000278, 0.2343750000000000278, 0.2348632812500000278, 0.2353515625000000278, 0.2358398437500000278, 0.2363281250000000278, 0.2368164062500000278, 0.2373046875000000278, 0.2377929687500000278, 0.2382812500000000278, 0.2387695312500000278, 0.2392578125000000278, 0.2397460937500000278, 0.2402343750000000278, 0.2407226562500000278, 0.2412109375000000278, 0.2416992187500000278, 0.2421875000000000278, 0.2426757812500000278, 0.2431640625000000278, 0.2436523437500000278, 0.2441406250000000278, 0.2446289062500000278, 0.2451171875000000278, 0.2456054687500000278, 0.2460937500000000278, 0.2465820312500000278, 0.2470703125000000278, 0.2475585937500000278, 0.2480468750000000278, 0.2485351562500000278, 0.2490234375000000278, 0.2495117187500000278, 0.2500000000000000000, 0.2504882812500000000, 0.2509765625000000000, 0.2514648437500000000, 0.2519531250000000000, 0.2524414062500000000, 0.2529296875000000000, 0.2534179687500000000, 0.2539062500000000000, 0.2543945312500000000, 0.2548828125000000000, 0.2553710937500000000, 0.2558593750000000000, 0.2563476562500000000, 0.2568359375000000000, 0.2573242187500000000, 0.2578125000000000000, 0.2583007812500000000, 0.2587890625000000000, 0.2592773437500000000, 0.2597656250000000000, 0.2602539062500000000, 0.2607421875000000000, 0.2612304687500000000, 0.2617187500000000000, 0.2622070312500000000, 0.2626953125000000000, 0.2631835937500000000, 0.2636718750000000000, 0.2641601562500000000, 0.2646484375000000000, 0.2651367187500000000, 0.2656250000000000000, 0.2661132812500000000, 0.2666015625000000000, 0.2670898437500000000, 0.2675781250000000000, 0.2680664062500000000, 0.2685546875000000000, 0.2690429687500000000, 0.2695312500000000000, 0.2700195312500000000, 0.2705078125000000000, 0.2709960937500000000, 0.2714843750000000000, 0.2719726562500000000, 0.2724609375000000000, 0.2729492187500000000, 0.2734375000000000000, 0.2739257812500000000, 0.2744140625000000000, 0.2749023437500000000, 0.2753906250000000000, 0.2758789062500000000, 0.2763671875000000000, 0.2768554687500000000, 0.2773437500000000000, 0.2778320312500000000, 0.2783203125000000000, 0.2788085937500000000, 0.2792968750000000000, 0.2797851562500000000, 0.2802734375000000000, 0.2807617187500000000, 0.2812500000000000000, 0.2817382812500000000, 0.2822265625000000000, 0.2827148437500000000, 0.2832031250000000000, 0.2836914062500000000, 0.2841796875000000000, 0.2846679687500000000, 0.2851562500000000000, 0.2856445312500000000, 0.2861328125000000000, 0.2866210937500000000, 0.2871093750000000000, 0.2875976562500000000, 0.2880859375000000000, 0.2885742187500000000, 0.2890625000000000000, 0.2895507812500000000, 0.2900390625000000000, 0.2905273437500000000, 0.2910156250000000000, 0.2915039062500000000, 0.2919921875000000000, 0.2924804687500000000, 0.2929687500000000000, 0.2934570312500000000, 0.2939453125000000000, 0.2944335937500000000, 0.2949218750000000000, 0.2954101562500000000, 0.2958984375000000000, 0.2963867187500000000, 0.2968750000000000000, 0.2973632812500000000, 0.2978515625000000000, 0.2983398437500000000, 0.2988281250000000000, 0.2993164062500000000, 0.2998046875000000000, 0.3002929687500000000, 0.3007812500000000000, 0.3012695312500000000, 0.3017578125000000000, 0.3022460937500000000, 0.3027343750000000000, 0.3032226562500000000, 0.3037109375000000000, 0.3041992187500000000, 0.3046875000000000000, 0.3051757812500000000, 0.3056640625000000000, 0.3061523437500000000, 0.3066406250000000000, 0.3071289062500000000, 0.3076171875000000000, 0.3081054687500000000, 0.3085937500000000000, 0.3090820312500000000, 0.3095703125000000000, 0.3100585937500000000, 0.3105468750000000000, 0.3110351562500000000, 0.3115234375000000000, 0.3120117187500000000, 0.3125000000000000000, 0.3129882812500000000, 0.3134765625000000000, 0.3139648437500000000, 0.3144531250000000000, 0.3149414062500000000, 0.3154296875000000000, 0.3159179687500000000, 0.3164062500000000000, 0.3168945312500000000, 0.3173828125000000000, 0.3178710937500000000, 0.3183593750000000000, 0.3188476562500000000, 0.3193359375000000000, 0.3198242187500000000, 0.3203125000000000000, 0.3208007812500000000, 0.3212890625000000000, 0.3217773437500000000, 0.3222656250000000000, 0.3227539062500000000, 0.3232421875000000000, 0.3237304687500000000, 0.3242187500000000000, 0.3247070312500000000, 0.3251953125000000000, 0.3256835937500000000, 0.3261718750000000000, 0.3266601562500000000, 0.3271484375000000000, 0.3276367187500000000, 0.3281250000000000000, 0.3286132812500000000, 0.3291015625000000000, 0.3295898437500000000, 0.3300781250000000000, 0.3305664062500000000, 0.3310546875000000000, 0.3315429687500000000, 0.3320312500000000000, 0.3325195312500000000, 0.3330078125000000000, 0.3334960937500000000, 0.3339843750000000000, 0.3344726562500000000, 0.3349609375000000000, 0.3354492187500000000, 0.3359375000000000000, 0.3364257812500000000, 0.3369140625000000000, 0.3374023437500000000, 0.3378906250000000000, 0.3383789062500000000, 0.3388671875000000000, 0.3393554687500000000, 0.3398437500000000000, 0.3403320312500000000, 0.3408203125000000000, 0.3413085937500000000, 0.3417968750000000000, 0.3422851562500000000, 0.3427734375000000000, 0.3432617187500000000, 0.3437500000000000000, 0.3442382812500000000, 0.3447265625000000000, 0.3452148437500000000, 0.3457031250000000000, 0.3461914062500000000, 0.3466796875000000000, 0.3471679687500000000, 0.3476562500000000000, 0.3481445312500000000, 0.3486328125000000000, 0.3491210937500000000, 0.3496093750000000000, 0.3500976562500000000, 0.3505859375000000000, 0.3510742187500000000, 0.3515625000000000000, 0.3520507812500000000, 0.3525390625000000000, 0.3530273437500000000, 0.3535156250000000000, 0.3540039062500000000, 0.3544921875000000000, 0.3549804687500000000, 0.3554687500000000000, 0.3559570312500000000, 0.3564453125000000000, 0.3569335937500000000, 0.3574218750000000000, 0.3579101562500000000, 0.3583984375000000000, 0.3588867187500000000, 0.3593750000000000000, 0.3598632812500000000, 0.3603515625000000000, 0.3608398437500000000, 0.3613281250000000000, 0.3618164062500000000, 0.3623046875000000000, 0.3627929687500000000, 0.3632812500000000000, 0.3637695312500000000, 0.3642578125000000000, 0.3647460937500000000, 0.3652343750000000000, 0.3657226562500000000, 0.3662109375000000000, 0.3666992187500000000, 0.3671875000000000000, 0.3676757812500000000, 0.3681640625000000000, 0.3686523437500000000, 0.3691406250000000000, 0.3696289062500000000, 0.3701171875000000000, 0.3706054687500000000, 0.3710937500000000000, 0.3715820312500000000, 0.3720703125000000000, 0.3725585937500000000, 0.3730468750000000000, 0.3735351562500000000, 0.3740234375000000000, 0.3745117187500000000, 0.3750000000000000000, 0.3754882812500000555, 0.3759765625000000555, 0.3764648437500000555, 0.3769531250000000555, 0.3774414062500000555, 0.3779296875000000555, 0.3784179687500000555, 0.3789062500000000555, 0.3793945312500000555, 0.3798828125000000555, 0.3803710937500000555, 0.3808593750000000555, 0.3813476562500000555, 0.3818359375000000555, 0.3823242187500000555, 0.3828125000000000555, 0.3833007812500000555, 0.3837890625000000555, 0.3842773437500000555, 0.3847656250000000555, 0.3852539062500000555, 0.3857421875000000555, 0.3862304687500000555, 0.3867187500000000555, 0.3872070312500000555, 0.3876953125000000555, 0.3881835937500000555, 0.3886718750000000555, 0.3891601562500000555, 0.3896484375000000555, 0.3901367187500000555, 0.3906250000000000555, 0.3911132812500000555, 0.3916015625000000555, 0.3920898437500000555, 0.3925781250000000555, 0.3930664062500000555, 0.3935546875000000555, 0.3940429687500000555, 0.3945312500000000555, 0.3950195312500000555, 0.3955078125000000555, 0.3959960937500000555, 0.3964843750000000555, 0.3969726562500000555, 0.3974609375000000555, 0.3979492187500000555, 0.3984375000000000555, 0.3989257812500000555, 0.3994140625000000555, 0.3999023437500000555, 0.4003906250000000555, 0.4008789062500000555, 0.4013671875000000555, 0.4018554687500000555, 0.4023437500000000555, 0.4028320312500000555, 0.4033203125000000555, 0.4038085937500000555, 0.4042968750000000555, 0.4047851562500000555, 0.4052734375000000555, 0.4057617187500000555, 0.4062500000000000555, 0.4067382812500000555, 0.4072265625000000555, 0.4077148437500000555, 0.4082031250000000555, 0.4086914062500000555, 0.4091796875000000555, 0.4096679687500000555, 0.4101562500000000555, 0.4106445312500000555, 0.4111328125000000555, 0.4116210937500000555, 0.4121093750000000555, 0.4125976562500000555, 0.4130859375000000555, 0.4135742187500000555, 0.4140625000000000555, 0.4145507812500000555, 0.4150390625000000555, 0.4155273437500000555, 0.4160156250000000555, 0.4165039062500000555, 0.4169921875000000555, 0.4174804687500000555, 0.4179687500000000555, 0.4184570312500000555, 0.4189453125000000555, 0.4194335937500000555, 0.4199218750000000555, 0.4204101562500000555, 0.4208984375000000555, 0.4213867187500000555, 0.4218750000000000555, 0.4223632812500000555, 0.4228515625000000555, 0.4233398437500000555, 0.4238281250000000555, 0.4243164062500000555, 0.4248046875000000555, 0.4252929687500000555, 0.4257812500000000555, 0.4262695312500000555, 0.4267578125000000555, 0.4272460937500000555, 0.4277343750000000555, 0.4282226562500000555, 0.4287109375000000555, 0.4291992187500000555, 0.4296875000000000555, 0.4301757812500000555, 0.4306640625000000555, 0.4311523437500000555, 0.4316406250000000555, 0.4321289062500000555, 0.4326171875000000555, 0.4331054687500000555, 0.4335937500000000555, 0.4340820312500000555, 0.4345703125000000555, 0.4350585937500000555, 0.4355468750000000555, 0.4360351562500000555, 0.4365234375000000555, 0.4370117187500000555, 0.4375000000000000555, 0.4379882812500000555, 0.4384765625000000555, 0.4389648437500000555, 0.4394531250000000555, 0.4399414062500000555, 0.4404296875000000555, 0.4409179687500000555, 0.4414062500000000555, 0.4418945312500000555, 0.4423828125000000555, 0.4428710937500000555, 0.4433593750000000555, 0.4438476562500000555, 0.4443359375000000555, 0.4448242187500000555, 0.4453125000000000555, 0.4458007812500000555, 0.4462890625000000555, 0.4467773437500000555, 0.4472656250000000555, 0.4477539062500000555, 0.4482421875000000555, 0.4487304687500000555, 0.4492187500000000555, 0.4497070312500000555, 0.4501953125000000555, 0.4506835937500000555, 0.4511718750000000555, 0.4516601562500000555, 0.4521484375000000555, 0.4526367187500000555, 0.4531250000000000555, 0.4536132812500000555, 0.4541015625000000555, 0.4545898437500000555, 0.4550781250000000555, 0.4555664062500000555, 0.4560546875000000555, 0.4565429687500000555, 0.4570312500000000555, 0.4575195312500000555, 0.4580078125000000555, 0.4584960937500000555, 0.4589843750000000555, 0.4594726562500000555, 0.4599609375000000555, 0.4604492187500000555, 0.4609375000000000555, 0.4614257812500000555, 0.4619140625000000555, 0.4624023437500000555, 0.4628906250000000555, 0.4633789062500000555, 0.4638671875000000555, 0.4643554687500000555, 0.4648437500000000555, 0.4653320312500000555, 0.4658203125000000555, 0.4663085937500000555, 0.4667968750000000555, 0.4672851562500000555, 0.4677734375000000555, 0.4682617187500000555, 0.4687500000000000555, 0.4692382812500000555, 0.4697265625000000555, 0.4702148437500000555, 0.4707031250000000555, 0.4711914062500000555, 0.4716796875000000555, 0.4721679687500000555, 0.4726562500000000555, 0.4731445312500000555, 0.4736328125000000555, 0.4741210937500000555, 0.4746093750000000555, 0.4750976562500000555, 0.4755859375000000555, 0.4760742187500000555, 0.4765625000000000555, 0.4770507812500000555, 0.4775390625000000555, 0.4780273437500000555, 0.4785156250000000555, 0.4790039062500000555, 0.4794921875000000555, 0.4799804687500000555, 0.4804687500000000555, 0.4809570312500000555, 0.4814453125000000555, 0.4819335937500000555, 0.4824218750000000555, 0.4829101562500000555, 0.4833984375000000555, 0.4838867187500000555, 0.4843750000000000555, 0.4848632812500000555, 0.4853515625000000555, 0.4858398437500000555, 0.4863281250000000555, 0.4868164062500000555, 0.4873046875000000555, 0.4877929687500000555, 0.4882812500000000555, 0.4887695312500000555, 0.4892578125000000555, 0.4897460937500000555, 0.4902343750000000555, 0.4907226562500000555, 0.4912109375000000555, 0.4916992187500000555, 0.4921875000000000555, 0.4926757812500000555, 0.4931640625000000555, 0.4936523437500000555, 0.4941406250000000555, 0.4946289062500000555, 0.4951171875000000555, 0.4956054687500000555, 0.4960937500000000555, 0.4965820312500000555, 0.4970703125000000555, 0.4975585937500000555, 0.4980468750000000555, 0.4985351562500000555, 0.4990234375000000555, 0.4995117187500000555, 0.5000000000000000000, 0.5004882812500000000, 0.5009765625000000000, 0.5014648437500000000, 0.5019531250000000000, 0.5024414062500000000, 0.5029296875000000000, 0.5034179687500000000, 0.5039062500000000000, 0.5043945312500000000, 0.5048828125000000000, 0.5053710937500000000, 0.5058593750000000000, 0.5063476562500000000, 0.5068359375000000000, 0.5073242187500000000, 0.5078125000000000000, 0.5083007812500000000, 0.5087890625000000000, 0.5092773437500000000, 0.5097656250000000000, 0.5102539062500000000, 0.5107421875000000000, 0.5112304687500000000, 0.5117187500000000000, 0.5122070312500000000, 0.5126953125000000000, 0.5131835937500000000, 0.5136718750000000000, 0.5141601562500000000, 0.5146484375000000000, 0.5151367187500000000, 0.5156250000000000000, 0.5161132812500000000, 0.5166015625000000000, 0.5170898437500000000, 0.5175781250000000000, 0.5180664062500000000, 0.5185546875000000000, 0.5190429687500000000, 0.5195312500000000000, 0.5200195312500000000, 0.5205078125000000000, 0.5209960937500000000, 0.5214843750000000000, 0.5219726562500000000, 0.5224609375000000000, 0.5229492187500000000, 0.5234375000000000000, 0.5239257812500000000, 0.5244140625000000000, 0.5249023437500000000, 0.5253906250000000000, 0.5258789062500000000, 0.5263671875000000000, 0.5268554687500000000, 0.5273437500000000000, 0.5278320312500000000, 0.5283203125000000000, 0.5288085937500000000, 0.5292968750000000000, 0.5297851562500000000, 0.5302734375000000000, 0.5307617187500000000, 0.5312500000000000000, 0.5317382812500000000, 0.5322265625000000000, 0.5327148437500000000, 0.5332031250000000000, 0.5336914062500000000, 0.5341796875000000000, 0.5346679687500000000, 0.5351562500000000000, 0.5356445312500000000, 0.5361328125000000000, 0.5366210937500000000, 0.5371093750000000000, 0.5375976562500000000, 0.5380859375000000000, 0.5385742187500000000, 0.5390625000000000000, 0.5395507812500000000, 0.5400390625000000000, 0.5405273437500000000, 0.5410156250000000000, 0.5415039062500000000, 0.5419921875000000000, 0.5424804687500000000, 0.5429687500000000000, 0.5434570312500000000, 0.5439453125000000000, 0.5444335937500000000, 0.5449218750000000000, 0.5454101562500000000, 0.5458984375000000000, 0.5463867187500000000, 0.5468750000000000000, 0.5473632812500000000, 0.5478515625000000000, 0.5483398437500000000, 0.5488281250000000000, 0.5493164062500000000, 0.5498046875000000000, 0.5502929687500000000, 0.5507812500000000000, 0.5512695312500000000, 0.5517578125000000000, 0.5522460937500000000, 0.5527343750000000000, 0.5532226562500000000, 0.5537109375000000000, 0.5541992187500000000, 0.5546875000000000000, 0.5551757812500000000, 0.5556640625000000000, 0.5561523437500000000, 0.5566406250000000000, 0.5571289062500000000, 0.5576171875000000000, 0.5581054687500000000, 0.5585937500000000000, 0.5590820312500000000, 0.5595703125000000000, 0.5600585937500000000, 0.5605468750000000000, 0.5610351562500000000, 0.5615234375000000000, 0.5620117187500000000, 0.5625000000000000000, 0.5629882812500000000, 0.5634765625000000000, 0.5639648437500000000, 0.5644531250000000000, 0.5649414062500000000, 0.5654296875000000000, 0.5659179687500000000, 0.5664062500000000000, 0.5668945312500000000, 0.5673828125000000000, 0.5678710937500000000, 0.5683593750000000000, 0.5688476562500000000, 0.5693359375000000000, 0.5698242187500000000, 0.5703125000000000000, 0.5708007812500000000, 0.5712890625000000000, 0.5717773437500000000, 0.5722656250000000000, 0.5727539062500000000, 0.5732421875000000000, 0.5737304687500000000, 0.5742187500000000000, 0.5747070312500000000, 0.5751953125000000000, 0.5756835937500000000, 0.5761718750000000000, 0.5766601562500000000, 0.5771484375000000000, 0.5776367187500000000, 0.5781250000000000000, 0.5786132812500000000, 0.5791015625000000000, 0.5795898437500000000, 0.5800781250000000000, 0.5805664062500000000, 0.5810546875000000000, 0.5815429687500000000, 0.5820312500000000000, 0.5825195312500000000, 0.5830078125000000000, 0.5834960937500000000, 0.5839843750000000000, 0.5844726562500000000, 0.5849609375000000000, 0.5854492187500000000, 0.5859375000000000000, 0.5864257812500000000, 0.5869140625000000000, 0.5874023437500000000, 0.5878906250000000000, 0.5883789062500000000, 0.5888671875000000000, 0.5893554687500000000, 0.5898437500000000000, 0.5903320312500000000, 0.5908203125000000000, 0.5913085937500000000, 0.5917968750000000000, 0.5922851562500000000, 0.5927734375000000000, 0.5932617187500000000, 0.5937500000000000000, 0.5942382812500000000, 0.5947265625000000000, 0.5952148437500000000, 0.5957031250000000000, 0.5961914062500000000, 0.5966796875000000000, 0.5971679687500000000, 0.5976562500000000000, 0.5981445312500000000, 0.5986328125000000000, 0.5991210937500000000, 0.5996093750000000000, 0.6000976562500000000, 0.6005859375000000000, 0.6010742187500000000, 0.6015625000000000000, 0.6020507812500000000, 0.6025390625000000000, 0.6030273437500000000, 0.6035156250000000000, 0.6040039062500000000, 0.6044921875000000000, 0.6049804687500000000, 0.6054687500000000000, 0.6059570312500000000, 0.6064453125000000000, 0.6069335937500000000, 0.6074218750000000000, 0.6079101562500000000, 0.6083984375000000000, 0.6088867187500000000, 0.6093750000000000000, 0.6098632812500000000, 0.6103515625000000000, 0.6108398437500000000, 0.6113281250000000000, 0.6118164062500000000, 0.6123046875000000000, 0.6127929687500000000, 0.6132812500000000000, 0.6137695312500000000, 0.6142578125000000000, 0.6147460937500000000, 0.6152343750000000000, 0.6157226562500000000, 0.6162109375000000000, 0.6166992187500000000, 0.6171875000000000000, 0.6176757812500000000, 0.6181640625000000000, 0.6186523437500000000, 0.6191406250000000000, 0.6196289062500000000, 0.6201171875000000000, 0.6206054687500000000, 0.6210937500000000000, 0.6215820312500000000, 0.6220703125000000000, 0.6225585937500000000, 0.6230468750000000000, 0.6235351562500000000, 0.6240234375000000000, 0.6245117187500000000, 0.6250000000000000000, 0.6254882812500000000, 0.6259765625000000000, 0.6264648437500000000, 0.6269531250000000000, 0.6274414062500000000, 0.6279296875000000000, 0.6284179687500000000, 0.6289062500000000000, 0.6293945312500000000, 0.6298828125000000000, 0.6303710937500000000, 0.6308593750000000000, 0.6313476562500000000, 0.6318359375000000000, 0.6323242187500000000, 0.6328125000000000000, 0.6333007812500000000, 0.6337890625000000000, 0.6342773437500000000, 0.6347656250000000000, 0.6352539062500000000, 0.6357421875000000000, 0.6362304687500000000, 0.6367187500000000000, 0.6372070312500000000, 0.6376953125000000000, 0.6381835937500000000, 0.6386718750000000000, 0.6391601562500000000, 0.6396484375000000000, 0.6401367187500000000, 0.6406250000000000000, 0.6411132812500000000, 0.6416015625000000000, 0.6420898437500000000, 0.6425781250000000000, 0.6430664062500000000, 0.6435546875000000000, 0.6440429687500000000, 0.6445312500000000000, 0.6450195312500000000, 0.6455078125000000000, 0.6459960937500000000, 0.6464843750000000000, 0.6469726562500000000, 0.6474609375000000000, 0.6479492187500000000, 0.6484375000000000000, 0.6489257812500000000, 0.6494140625000000000, 0.6499023437500000000, 0.6503906250000000000, 0.6508789062500000000, 0.6513671875000000000, 0.6518554687500000000, 0.6523437500000000000, 0.6528320312500000000, 0.6533203125000000000, 0.6538085937500000000, 0.6542968750000000000, 0.6547851562500000000, 0.6552734375000000000, 0.6557617187500000000, 0.6562500000000000000, 0.6567382812500000000, 0.6572265625000000000, 0.6577148437500000000, 0.6582031250000000000, 0.6586914062500000000, 0.6591796875000000000, 0.6596679687500000000, 0.6601562500000000000, 0.6606445312500000000, 0.6611328125000000000, 0.6616210937500000000, 0.6621093750000000000, 0.6625976562500000000, 0.6630859375000000000, 0.6635742187500000000, 0.6640625000000000000, 0.6645507812500000000, 0.6650390625000000000, 0.6655273437500000000, 0.6660156250000000000, 0.6665039062500000000, 0.6669921875000000000, 0.6674804687500000000, 0.6679687500000000000, 0.6684570312500000000, 0.6689453125000000000, 0.6694335937500000000, 0.6699218750000000000, 0.6704101562500000000, 0.6708984375000000000, 0.6713867187500000000, 0.6718750000000000000, 0.6723632812500000000, 0.6728515625000000000, 0.6733398437500000000, 0.6738281250000000000, 0.6743164062500000000, 0.6748046875000000000, 0.6752929687500000000, 0.6757812500000000000, 0.6762695312500000000, 0.6767578125000000000, 0.6772460937500000000, 0.6777343750000000000, 0.6782226562500000000, 0.6787109375000000000, 0.6791992187500000000, 0.6796875000000000000, 0.6801757812500000000, 0.6806640625000000000, 0.6811523437500000000, 0.6816406250000000000, 0.6821289062500000000, 0.6826171875000000000, 0.6831054687500000000, 0.6835937500000000000, 0.6840820312500000000, 0.6845703125000000000, 0.6850585937500000000, 0.6855468750000000000, 0.6860351562500000000, 0.6865234375000000000, 0.6870117187500000000, 0.6875000000000000000, 0.6879882812500000000, 0.6884765625000000000, 0.6889648437500000000, 0.6894531250000000000, 0.6899414062500000000, 0.6904296875000000000, 0.6909179687500000000, 0.6914062500000000000, 0.6918945312500000000, 0.6923828125000000000, 0.6928710937500000000, 0.6933593750000000000, 0.6938476562500000000, 0.6943359375000000000, 0.6948242187500000000, 0.6953125000000000000, 0.6958007812500000000, 0.6962890625000000000, 0.6967773437500000000, 0.6972656250000000000, 0.6977539062500000000, 0.6982421875000000000, 0.6987304687500000000, 0.6992187500000000000, 0.6997070312500000000, 0.7001953125000000000, 0.7006835937500000000, 0.7011718750000000000, 0.7016601562500000000, 0.7021484375000000000, 0.7026367187500000000, 0.7031250000000000000, 0.7036132812500000000, 0.7041015625000000000, 0.7045898437500000000, 0.7050781250000000000, 0.7055664062500000000, 0.7060546875000000000, 0.7065429687500000000, 0.7070312500000000000, 0.7075195312500000000, 0.7080078125000000000, 0.7084960937500000000, 0.7089843750000000000, 0.7094726562500000000, 0.7099609375000000000, 0.7104492187500000000, 0.7109375000000000000, 0.7114257812500000000, 0.7119140625000000000, 0.7124023437500000000, 0.7128906250000000000, 0.7133789062500000000, 0.7138671875000000000, 0.7143554687500000000, 0.7148437500000000000, 0.7153320312500000000, 0.7158203125000000000, 0.7163085937500000000, 0.7167968750000000000, 0.7172851562500000000, 0.7177734375000000000, 0.7182617187500000000, 0.7187500000000000000, 0.7192382812500000000, 0.7197265625000000000, 0.7202148437500000000, 0.7207031250000000000, 0.7211914062500000000, 0.7216796875000000000, 0.7221679687500000000, 0.7226562500000000000, 0.7231445312500000000, 0.7236328125000000000, 0.7241210937500000000, 0.7246093750000000000, 0.7250976562500000000, 0.7255859375000000000, 0.7260742187500000000, 0.7265625000000000000, 0.7270507812500000000, 0.7275390625000000000, 0.7280273437500000000, 0.7285156250000000000, 0.7290039062500000000, 0.7294921875000000000, 0.7299804687500000000, 0.7304687500000000000, 0.7309570312500000000, 0.7314453125000000000, 0.7319335937500000000, 0.7324218750000000000, 0.7329101562500000000, 0.7333984375000000000, 0.7338867187500000000, 0.7343750000000000000, 0.7348632812500000000, 0.7353515625000000000, 0.7358398437500000000, 0.7363281250000000000, 0.7368164062500000000, 0.7373046875000000000, 0.7377929687500000000, 0.7382812500000000000, 0.7387695312500000000, 0.7392578125000000000, 0.7397460937500000000, 0.7402343750000000000, 0.7407226562500000000, 0.7412109375000000000, 0.7416992187500000000, 0.7421875000000000000, 0.7426757812500000000, 0.7431640625000000000, 0.7436523437500000000, 0.7441406250000000000, 0.7446289062500000000, 0.7451171875000000000, 0.7456054687500000000, 0.7460937500000000000, 0.7465820312500000000, 0.7470703125000000000, 0.7475585937500000000, 0.7480468750000000000, 0.7485351562500000000, 0.7490234375000000000, 0.7495117187500000000, 0.7500000000000000000, 0.7504882812500001110, 0.7509765625000001110, 0.7514648437500001110, 0.7519531250000001110, 0.7524414062500001110, 0.7529296875000001110, 0.7534179687500001110, 0.7539062500000001110, 0.7543945312500001110, 0.7548828125000001110, 0.7553710937500001110, 0.7558593750000001110, 0.7563476562500001110, 0.7568359375000001110, 0.7573242187500001110, 0.7578125000000001110, 0.7583007812500001110, 0.7587890625000001110, 0.7592773437500001110, 0.7597656250000001110, 0.7602539062500001110, 0.7607421875000001110, 0.7612304687500001110, 0.7617187500000001110, 0.7622070312500001110, 0.7626953125000001110, 0.7631835937500001110, 0.7636718750000001110, 0.7641601562500001110, 0.7646484375000001110, 0.7651367187500001110, 0.7656250000000001110, 0.7661132812500001110, 0.7666015625000001110, 0.7670898437500001110, 0.7675781250000001110, 0.7680664062500001110, 0.7685546875000001110, 0.7690429687500001110, 0.7695312500000001110, 0.7700195312500001110, 0.7705078125000001110, 0.7709960937500001110, 0.7714843750000001110, 0.7719726562500001110, 0.7724609375000001110, 0.7729492187500001110, 0.7734375000000001110, 0.7739257812500001110, 0.7744140625000001110, 0.7749023437500001110, 0.7753906250000001110, 0.7758789062500001110, 0.7763671875000001110, 0.7768554687500001110, 0.7773437500000001110, 0.7778320312500001110, 0.7783203125000001110, 0.7788085937500001110, 0.7792968750000001110, 0.7797851562500001110, 0.7802734375000001110, 0.7807617187500001110, 0.7812500000000001110, 0.7817382812500001110, 0.7822265625000001110, 0.7827148437500001110, 0.7832031250000001110, 0.7836914062500001110, 0.7841796875000001110, 0.7846679687500001110, 0.7851562500000001110, 0.7856445312500001110, 0.7861328125000001110, 0.7866210937500001110, 0.7871093750000001110, 0.7875976562500001110, 0.7880859375000001110, 0.7885742187500001110, 0.7890625000000001110, 0.7895507812500001110, 0.7900390625000001110, 0.7905273437500001110, 0.7910156250000001110, 0.7915039062500001110, 0.7919921875000001110, 0.7924804687500001110, 0.7929687500000001110, 0.7934570312500001110, 0.7939453125000001110, 0.7944335937500001110, 0.7949218750000001110, 0.7954101562500001110, 0.7958984375000001110, 0.7963867187500001110, 0.7968750000000001110, 0.7973632812500001110, 0.7978515625000001110, 0.7983398437500001110, 0.7988281250000001110, 0.7993164062500001110, 0.7998046875000001110, 0.8002929687500001110, 0.8007812500000001110, 0.8012695312500001110, 0.8017578125000001110, 0.8022460937500001110, 0.8027343750000001110, 0.8032226562500001110, 0.8037109375000001110, 0.8041992187500001110, 0.8046875000000001110, 0.8051757812500001110, 0.8056640625000001110, 0.8061523437500001110, 0.8066406250000001110, 0.8071289062500001110, 0.8076171875000001110, 0.8081054687500001110, 0.8085937500000001110, 0.8090820312500001110, 0.8095703125000001110, 0.8100585937500001110, 0.8105468750000001110, 0.8110351562500001110, 0.8115234375000001110, 0.8120117187500001110, 0.8125000000000001110, 0.8129882812500001110, 0.8134765625000001110, 0.8139648437500001110, 0.8144531250000001110, 0.8149414062500001110, 0.8154296875000001110, 0.8159179687500001110, 0.8164062500000001110, 0.8168945312500001110, 0.8173828125000001110, 0.8178710937500001110, 0.8183593750000001110, 0.8188476562500001110, 0.8193359375000001110, 0.8198242187500001110, 0.8203125000000001110, 0.8208007812500001110, 0.8212890625000001110, 0.8217773437500001110, 0.8222656250000001110, 0.8227539062500001110, 0.8232421875000001110, 0.8237304687500001110, 0.8242187500000001110, 0.8247070312500001110, 0.8251953125000001110, 0.8256835937500001110, 0.8261718750000001110, 0.8266601562500001110, 0.8271484375000001110, 0.8276367187500001110, 0.8281250000000001110, 0.8286132812500001110, 0.8291015625000001110, 0.8295898437500001110, 0.8300781250000001110, 0.8305664062500001110, 0.8310546875000001110, 0.8315429687500001110, 0.8320312500000001110, 0.8325195312500001110, 0.8330078125000001110, 0.8334960937500001110, 0.8339843750000001110, 0.8344726562500001110, 0.8349609375000001110, 0.8354492187500001110, 0.8359375000000001110, 0.8364257812500001110, 0.8369140625000001110, 0.8374023437500001110, 0.8378906250000001110, 0.8383789062500001110, 0.8388671875000001110, 0.8393554687500001110, 0.8398437500000001110, 0.8403320312500001110, 0.8408203125000001110, 0.8413085937500001110, 0.8417968750000001110, 0.8422851562500001110, 0.8427734375000001110, 0.8432617187500001110, 0.8437500000000001110, 0.8442382812500001110, 0.8447265625000001110, 0.8452148437500001110, 0.8457031250000001110, 0.8461914062500001110, 0.8466796875000001110, 0.8471679687500001110, 0.8476562500000001110, 0.8481445312500001110, 0.8486328125000001110, 0.8491210937500001110, 0.8496093750000001110, 0.8500976562500001110, 0.8505859375000001110, 0.8510742187500001110, 0.8515625000000001110, 0.8520507812500001110, 0.8525390625000001110, 0.8530273437500001110, 0.8535156250000001110, 0.8540039062500001110, 0.8544921875000001110, 0.8549804687500001110, 0.8554687500000001110, 0.8559570312500001110, 0.8564453125000001110, 0.8569335937500001110, 0.8574218750000001110, 0.8579101562500001110, 0.8583984375000001110, 0.8588867187500001110, 0.8593750000000001110, 0.8598632812500001110, 0.8603515625000001110, 0.8608398437500001110, 0.8613281250000001110, 0.8618164062500001110, 0.8623046875000001110, 0.8627929687500001110, 0.8632812500000001110, 0.8637695312500001110, 0.8642578125000001110, 0.8647460937500001110, 0.8652343750000001110, 0.8657226562500001110, 0.8662109375000001110, 0.8666992187500001110, 0.8671875000000001110, 0.8676757812500001110, 0.8681640625000001110, 0.8686523437500001110, 0.8691406250000001110, 0.8696289062500001110, 0.8701171875000001110, 0.8706054687500001110, 0.8710937500000001110, 0.8715820312500001110, 0.8720703125000001110, 0.8725585937500001110, 0.8730468750000001110, 0.8735351562500001110, 0.8740234375000001110, 0.8745117187500001110, 0.8750000000000001110, 0.8754882812500001110, 0.8759765625000001110, 0.8764648437500001110, 0.8769531250000001110, 0.8774414062500001110, 0.8779296875000001110, 0.8784179687500001110, 0.8789062500000001110, 0.8793945312500001110, 0.8798828125000001110, 0.8803710937500001110, 0.8808593750000001110, 0.8813476562500001110, 0.8818359375000001110, 0.8823242187500001110, 0.8828125000000001110, 0.8833007812500001110, 0.8837890625000001110, 0.8842773437500001110, 0.8847656250000001110, 0.8852539062500001110, 0.8857421875000001110, 0.8862304687500001110, 0.8867187500000001110, 0.8872070312500001110, 0.8876953125000001110, 0.8881835937500001110, 0.8886718750000001110, 0.8891601562500001110, 0.8896484375000001110, 0.8901367187500001110, 0.8906250000000001110, 0.8911132812500001110, 0.8916015625000001110, 0.8920898437500001110, 0.8925781250000001110, 0.8930664062500001110, 0.8935546875000001110, 0.8940429687500001110, 0.8945312500000001110, 0.8950195312500001110, 0.8955078125000001110, 0.8959960937500001110, 0.8964843750000001110, 0.8969726562500001110, 0.8974609375000001110, 0.8979492187500001110, 0.8984375000000001110, 0.8989257812500001110, 0.8994140625000001110, 0.8999023437500001110, 0.9003906250000001110, 0.9008789062500001110, 0.9013671875000001110, 0.9018554687500001110, 0.9023437500000001110, 0.9028320312500001110, 0.9033203125000001110, 0.9038085937500001110, 0.9042968750000001110, 0.9047851562500001110, 0.9052734375000001110, 0.9057617187500001110, 0.9062500000000001110, 0.9067382812500001110, 0.9072265625000001110, 0.9077148437500001110, 0.9082031250000001110, 0.9086914062500001110, 0.9091796875000001110, 0.9096679687500001110, 0.9101562500000001110, 0.9106445312500001110, 0.9111328125000001110, 0.9116210937500001110, 0.9121093750000001110, 0.9125976562500001110, 0.9130859375000001110, 0.9135742187500001110, 0.9140625000000001110, 0.9145507812500001110, 0.9150390625000001110, 0.9155273437500001110, 0.9160156250000001110, 0.9165039062500001110, 0.9169921875000001110, 0.9174804687500001110, 0.9179687500000001110, 0.9184570312500001110, 0.9189453125000001110, 0.9194335937500001110, 0.9199218750000001110, 0.9204101562500001110, 0.9208984375000001110, 0.9213867187500001110, 0.9218750000000001110, 0.9223632812500001110, 0.9228515625000001110, 0.9233398437500001110, 0.9238281250000001110, 0.9243164062500001110, 0.9248046875000001110, 0.9252929687500001110, 0.9257812500000001110, 0.9262695312500001110, 0.9267578125000001110, 0.9272460937500001110, 0.9277343750000001110, 0.9282226562500001110, 0.9287109375000001110, 0.9291992187500001110, 0.9296875000000001110, 0.9301757812500001110, 0.9306640625000001110, 0.9311523437500001110, 0.9316406250000001110, 0.9321289062500001110, 0.9326171875000001110, 0.9331054687500001110, 0.9335937500000001110, 0.9340820312500001110, 0.9345703125000001110, 0.9350585937500001110, 0.9355468750000001110, 0.9360351562500001110, 0.9365234375000001110, 0.9370117187500001110, 0.9375000000000001110, 0.9379882812500001110, 0.9384765625000001110, 0.9389648437500001110, 0.9394531250000001110, 0.9399414062500001110, 0.9404296875000001110, 0.9409179687500001110, 0.9414062500000001110, 0.9418945312500001110, 0.9423828125000001110, 0.9428710937500001110, 0.9433593750000001110, 0.9438476562500001110, 0.9443359375000001110, 0.9448242187500001110, 0.9453125000000001110, 0.9458007812500001110, 0.9462890625000001110, 0.9467773437500001110, 0.9472656250000001110, 0.9477539062500001110, 0.9482421875000001110, 0.9487304687500001110, 0.9492187500000001110, 0.9497070312500001110, 0.9501953125000001110, 0.9506835937500001110, 0.9511718750000001110, 0.9516601562500001110, 0.9521484375000001110, 0.9526367187500001110, 0.9531250000000001110, 0.9536132812500001110, 0.9541015625000001110, 0.9545898437500001110, 0.9550781250000001110, 0.9555664062500001110, 0.9560546875000001110, 0.9565429687500001110, 0.9570312500000001110, 0.9575195312500001110, 0.9580078125000001110, 0.9584960937500001110, 0.9589843750000001110, 0.9594726562500001110, 0.9599609375000001110, 0.9604492187500001110, 0.9609375000000001110, 0.9614257812500001110, 0.9619140625000001110, 0.9624023437500001110, 0.9628906250000001110, 0.9633789062500001110, 0.9638671875000001110, 0.9643554687500001110, 0.9648437500000001110, 0.9653320312500001110, 0.9658203125000001110, 0.9663085937500001110, 0.9667968750000001110, 0.9672851562500001110, 0.9677734375000001110, 0.9682617187500001110, 0.9687500000000001110, 0.9692382812500001110, 0.9697265625000001110, 0.9702148437500001110, 0.9707031250000001110, 0.9711914062500001110, 0.9716796875000001110, 0.9721679687500001110, 0.9726562500000001110, 0.9731445312500001110, 0.9736328125000001110, 0.9741210937500001110, 0.9746093750000001110, 0.9750976562500001110, 0.9755859375000001110, 0.9760742187500001110, 0.9765625000000001110, 0.9770507812500001110, 0.9775390625000001110, 0.9780273437500001110, 0.9785156250000001110, 0.9790039062500001110, 0.9794921875000001110, 0.9799804687500001110, 0.9804687500000001110, 0.9809570312500001110, 0.9814453125000001110, 0.9819335937500001110, 0.9824218750000001110, 0.9829101562500001110, 0.9833984375000001110, 0.9838867187500001110, 0.9843750000000001110, 0.9848632812500001110, 0.9853515625000001110, 0.9858398437500001110, 0.9863281250000001110, 0.9868164062500001110, 0.9873046875000001110, 0.9877929687500001110, 0.9882812500000001110, 0.9887695312500001110, 0.9892578125000001110, 0.9897460937500001110, 0.9902343750000001110, 0.9907226562500001110, 0.9912109375000001110, 0.9916992187500001110, 0.9921875000000001110, 0.9926757812500001110, 0.9931640625000001110, 0.9936523437500001110, 0.9941406250000001110, 0.9946289062500001110, 0.9951171875000001110, 0.9956054687500001110, 0.9960937500000001110, 0.9965820312500001110, 0.9970703125000001110, 0.9975585937500001110, 0.9980468750000001110, 0.9985351562500001110, 0.9990234375000001110, 0.9995117187500001110, 1.000000000000000000 ),
 .UNSPECIFIED. ) ;
#78055=CARTESIAN_POINT ( 'NONE',  ( 19.22361159462649027, -4.937694622890139939, 11.49999999999999645 ) ) ;
#78056=CARTESIAN_POINT ( 'NONE',  ( -48.62287095715004881, -24.65952944569303895, 1.056160979905692798 ) ) ;
#78058=PLANE ( 'NONE',  #30981 ) ;
#78062=CARTESIAN_POINT ( 'NONE',  ( -80.52287095715006160, -23.47596703998600631, 11.44779298504228571 ) ) ;
#78064=CARTESIAN_POINT ( 'NONE',  ( -51.60452015029387951, -25.10935914944338165, 3.558373330915750810 ) ) ;
#78065=CARTESIAN_POINT ( 'NONE',  ( -2.129050106866105185, 21.58297100922832357, 11.49999999999998934 ) ) ;
#78066=CARTESIAN_POINT ( 'NONE',  ( -29.62287095715006302, -23.87261080661619062, 10.65372852762611622 ) ) ;
#78067=CARTESIAN_POINT ( 'NONE',  ( 8.918240691521024388, 17.32521578647535776, -1.500000000000002220 ) ) ;
#78072=CARTESIAN_POINT ( 'NONE',  ( -9.549598871097368047, 18.00506641634745009, 11.49999999999999645 ) ) ;
#78073=CARTESIAN_POINT ( 'NONE',  ( -80.62882275262062137, -24.73486907724918282, 1.287355809206963908 ) ) ;
#78074=EDGE_CURVE ( 'NONE', #52671, #5568, #38287, .T. ) ;
#78075=DIRECTION ( 'NONE',  ( 0.000000000000000000, 0.9999999999976377785, 2.173523156925979975E-06 ) ) ;
#78076=EDGE_CURVE ( 'NONE', #76732, #59182, #56479, .T. ) ;
#78079=CARTESIAN_POINT ( 'NONE',  ( -35.62287095715005592, -29.50250243563736774, 8.947779886222148704 ) ) ;
#78080=CARTESIAN_POINT ( 'NONE',  ( -48.87380231474225667, -25.25214687568168870, 6.137092009077116828 ) ) ;
#78081=CARTESIAN_POINT ( 'NONE',  ( -40.47157810787772547, -24.92592662359560762, 8.075495903017996469 ) ) ;
#78082=PLANE ( 'NONE',  #20327 ) ;
#78083=CARTESIAN_POINT ( 'NONE',  ( 10.01938154005162218, -17.43019892170380913, 11.49999999999998934 ) ) ;
#78085=CARTESIAN_POINT ( 'NONE',  ( -45.62287095715004881, -23.47593901973091235, -1.443836447539009749 ) ) ;
#78086=ORIENTED_EDGE ( 'NONE', *, *, #34917, .F. ) ;
#78087=CARTESIAN_POINT ( 'NONE',  ( -36.52287095715006870, -23.47593901973090169, -1.443836447538997314 ) ) ;
#78088=EDGE_CURVE ( 'NONE', #70270, #95088, #48021, .T. ) ;
#78089=CARTESIAN_POINT ( 'NONE',  ( 21.91704834537361180, 6.644925864936762849, 11.49999999999999645 ) ) ;
#78090=CARTESIAN_POINT ( 'NONE',  ( 18.72737137862276313, -12.84423604280260278, 11.49999999999998934 ) ) ;
#78091=VERTEX_POINT ( 'NONE', #56902 ) ;
#78092=CARTESIAN_POINT ( 'NONE',  ( -53.62287095715005592, -24.66019654487199375, 8.947790411086135265 ) ) ;
#78093=CARTESIAN_POINT ( 'NONE',  ( -95.52287095715006160, -29.50248789122583659, 2.256150453626215580 ) ) ;
#78094=CARTESIAN_POINT ( 'NONE',  ( -39.45282898296882479, -25.27930806443914591, 4.061648798908704450 ) ) ;
#78095=CARTESIAN_POINT ( 'NONE',  ( -30.57287095715005520, -25.10878950975746804, 7.249410248868700002 ) ) ;
#78096=CARTESIAN_POINT ( 'NONE',  ( -128.5901391630868318, -23.73791477778912196, 11.05961554403169522 ) ) ;
#78098=B_SPLINE_CURVE_WITH_KNOTS ( 'NONE', 3,
 ( #60207, #20129, #89647, #13504 ),
 .UNSPECIFIED., .F., .F.,
 ( 4, 4 ),
 ( 0.000000000000000000, 9.999999999998206125E-05 ),
 .UNSPECIFIED. ) ;
#78099=CARTESIAN_POINT ( 'NONE',  ( -98.89303308397303738, -25.25460725902716774, 6.110950176806278833 ) ) ;
#78101=CARTESIAN_POINT ( 'NONE',  ( 20.39576089869593289, -0.2533167397448486957, 11.49999999999998934 ) ) ;
#78102=ORIENTED_EDGE ( 'NONE', *, *, #73811, .T. ) ;
#78103=CARTESIAN_POINT ( 'NONE',  ( 3.160899137004691717, 22.77513019406404382, -1.500000000000002220 ) ) ;
#78105=CARTESIAN_POINT ( 'NONE',  ( -54.49651346487743098, -24.35071581493543391, 9.817618358456034144 ) ) ;
#78106=ORIENTED_EDGE ( 'NONE', *, *, #86831, .T. ) ;
#78107=CARTESIAN_POINT ( 'NONE',  ( -110.9909297185884327, -25.15277794460069671, 6.986250878905948980 ) ) ;
#78108=EDGE_CURVE ( 'NONE', #63195, #85963, #2014, .T. ) ;
#78109=CARTESIAN_POINT ( 'NONE',  ( -53.53250099041933652, -24.66019654487199375, 8.947790411086122830 ) ) ;
#78110=CARTESIAN_POINT ( 'NONE',  ( 12.49974722350246736, 17.29906535522423638, 11.49999999999999645 ) ) ;
#78113=ORIENTED_EDGE ( 'NONE', *, *, #76312, .F. ) ;
#78114=CARTESIAN_POINT ( 'NONE',  ( -21.66996937300057269, -4.939502015459471096, -1.500000000000002220 ) ) ;
#78116=CARTESIAN_POINT ( 'NONE',  ( -7.851838630353038972, -19.11370409007043847, -1.500000000000002220 ) ) ;
#78117=EDGE_LOOP ( 'NONE', ( #2190, #14592, #87114, #13617 ) ) ;
#78118=EDGE_CURVE ( 'NONE', #18750, #7644, #58396, .T. ) ;
#78119=CARTESIAN_POINT ( 'NONE',  ( -108.9545715455115129, -25.27682575596922021, 4.170144840047737667 ) ) ;
#78120=CARTESIAN_POINT ( 'NONE',  ( -95.50376022624848815, -24.83644354573579349, 8.397322867130096569 ) ) ;
#78122=CARTESIAN_POINT ( 'NONE',  ( -83.62287095715007013, -23.47596703998600631, 11.44779298504227860 ) ) ;
#78125=CARTESIAN_POINT ( 'NONE',  ( -48.52287095715006160, -24.64898659630367561, 1.056161002820821038 ) ) ;
#78126=CARTESIAN_POINT ( 'NONE',  ( 4.013313563623547964, -20.52093592976233438, -1.500000000000002220 ) ) ;
#78127=CARTESIAN_POINT ( 'NONE',  ( -18.25314811174894913, -11.95880190493418738, 11.49999999999999645 ) ) ;
#78128=CARTESIAN_POINT ( 'NONE',  ( -44.62287095715004881, -29.50250243563736774, 8.947779886222148704 ) ) ;
#78129=CARTESIAN_POINT ( 'NONE',  ( -99.50401037219587863, -25.08800262214248988, 7.296243261531031088 ) ) ;
#78130=CARTESIAN_POINT ( 'NONE',  ( 22.01961411883556252, 4.383451955130949429, 11.49999999999998934 ) ) ;
#78131=FACE_OUTER_BOUND ( 'NONE', #57820, .T. ) ;
#78132=CARTESIAN_POINT ( 'NONE',  ( -58.52287095715006160, -24.34917612406836440, 0.1852690917426536021 ) ) ;
#78133=AXIS2_PLACEMENT_3D ( 'NONE', #16557, #847, #56152 ) ;
#78134=CARTESIAN_POINT ( 'NONE',  ( -54.62287095715005592, -24.65952944569304606, 1.056160979905694131 ) ) ;
#78135=PRODUCT_DEFINITION_FORMATION_WITH_SPECIFIED_SOURCE ( 'ANY', '', #20704, .NOT_KNOWN. ) ;
#78137=EDGE_LOOP ( 'NONE', ( #60766, #37576, #9143, #73607 ) ) ;
#78141=CARTESIAN_POINT ( 'NONE',  ( 4.555389213293416617, -20.86945110937667280, -1.500000000000002220 ) ) ;
#78142=CARTESIAN_POINT ( 'NONE',  ( -7.019573500991415749, 21.25910006591672996, 11.49999999999999645 ) ) ;
#78144=CARTESIAN_POINT ( 'NONE',  ( 12.48895993392301307, -16.95307763291877379, 11.49999999999998934 ) ) ;
#78145=CARTESIAN_POINT ( 'NONE',  ( -30.59774034470085624, -24.76209092868932160, 1.363670884829966123 ) ) ;
#78146=CARTESIAN_POINT ( 'NONE',  ( -18.10700488460823721, -8.296952762055457953, -1.500000000000002220 ) ) ;
#78147=LINE ( 'NONE', #94890, #50157 ) ;
#78149=CARTESIAN_POINT ( 'NONE',  ( -20.58003014649542095, 7.718188279156099618, -1.500000000000002220 ) ) ;
#78151=VECTOR ( 'NONE', #42737, 1000.000000000000114 ) ;
#78152=VERTEX_POINT ( 'NONE', #50277 ) ;
#78153=CARTESIAN_POINT ( 'NONE',  ( -104.6228709571500559, -29.50248528299804818, 1.056150453629042030 ) ) ;
#78155=CARTESIAN_POINT ( 'NONE',  ( -121.5228709571500474, -24.50216790748205398, 0.6166512839542598323 ) ) ;
#78156=CARTESIAN_POINT ( 'NONE',  ( 8.324980675869593227, 19.10421180063631752, 11.49999999999999645 ) ) ;
#78162=CARTESIAN_POINT ( 'NONE',  ( -90.52287095715006160, -25.00158670708909625, 2.256160236439166411 ) ) ;
#78163=CARTESIAN_POINT ( 'NONE',  ( -4.607724273132460802, 20.83226218841027944, 11.49999999999998934 ) ) ;
#78164=CARTESIAN_POINT ( 'NONE',  ( -98.59636631811120822, -23.73791477778911840, 11.05961554403170410 ) ) ;
#78165=DIRECTION ( 'NONE',  ( 0.000000000000000000, -2.173523156925979552E-06, 0.9999999999976378895 ) ) ;
#78167=CARTESIAN_POINT ( 'NONE',  ( -69.32992225813151776, -25.30188801935125653, 5.302352381037461093 ) ) ;
#78168=B_SPLINE_CURVE_WITH_KNOTS ( 'NONE', 3,
 ( #86017, #72806, #16494, #63712, #47967, #65217 ),
 .UNSPECIFIED., .F., .F.,
 ( 4, 2, 4 ),
 ( 0.000000000000000000, 0.001380901958385387894, 0.002761803916770775788 ),
 .UNSPECIFIED. ) ;
#78169=CARTESIAN_POINT ( 'NONE',  ( 17.87336509531889561, -13.68139028912531785, -1.500000000000002220 ) ) ;
#78171=B_SPLINE_SURFACE_WITH_KNOTS ( 'NONE', 3, 1, ( 
 ( #70726, #48395 ),
 ( #62125, #100141 ),
 ( #56016, #23025 ),
 ( #39268, #63129 ),
 ( #15926, #84943 ),
 ( #71232, #46893 ),
 ( #77320, #77811 ),
 ( #24541, #38767 ),
 ( #70228, #708 ),
 ( #79329, #61633 ),
 ( #93047, #31654 ) ),
 .UNSPECIFIED., .F., .F., .F.,
 ( 4, 1, 1, 1, 1, 1, 1, 1, 4 ),
 ( 2, 2 ),
 ( 0.000000000000000000, 0.1280675485958910620, 0.2506083188676687667, 0.3706301659145028737, 0.4900722467299511442, 0.6103747641546218849, 0.7343130699115234528, 0.8632165042449871928, 1.000000000000000000 ),
 ( 0.000000000000000000, 1.000000000000000000 ),
 .UNSPECIFIED. ) ;
#78172=DIRECTION ( 'NONE',  ( -3.773278334444167608E-23, 1.000000000000000000, 0.000000000000000000 ) ) ;
#78173=ORIENTED_EDGE ( 'NONE', *, *, #11204, .F. ) ;
#78174=CARTESIAN_POINT ( 'NONE',  ( -78.94971039626406650, -25.28065224745481032, 5.786440773245404401 ) ) ;
#78175=CARTESIAN_POINT ( 'NONE',  ( -81.62287095715005592, -24.64965695001468404, 8.947790433994182280 ) ) ;
#78176=CARTESIAN_POINT ( 'NONE',  ( 16.89532177248590372, -10.13005384644002227, 11.49999999999999645 ) ) ;
#78178=CARTESIAN_POINT ( 'NONE',  ( -119.5228709571500758, -23.47596703998600631, 11.44779298504227860 ) ) ;
#78179=B_SPLINE_CURVE_WITH_KNOTS ( 'NONE', 3,
 ( #56782, #87717, #18199, #95817, #45539, #60273 ),
 .UNSPECIFIED., .F., .F.,
 ( 4, 2, 4 ),
 ( 6.384118678608962257E-06, 0.001386860460828373467, 0.002767336802978137989 ),
 .UNSPECIFIED. ) ;
#78180=ADVANCED_FACE ( 'NONE', ( #28416 ), #18810, .T. ) ;
#78181=EDGE_CURVE ( 'NONE', #78336, #77156, #68495, .T. ) ;
#78184=CARTESIAN_POINT ( 'NONE',  ( -58.62287095715004881, -29.50247984919015209, -1.443849546365056913 ) ) ;
#78185=CARTESIAN_POINT ( 'NONE',  ( -52.52287095715005449, -23.47593901973090524, -1.443836447538997092 ) ) ;
#78187=CARTESIAN_POINT ( 'NONE',  ( 0.5484783294719396407, -19.75002165935583776, -1.500000000000002220 ) ) ;
#78191=EDGE_CURVE ( 'NONE', #26463, #98147, #11701, .T. ) ;
#78193=ORIENTED_EDGE ( 'NONE', *, *, #69966, .T. ) ;
#78194=PLANE ( 'NONE',  #1403 ) ;
#78195=CARTESIAN_POINT ( 'NONE',  ( -53.62287095715005592, -23.47593901973091235, -1.443836447539009749 ) ) ;
#78196=CARTESIAN_POINT ( 'NONE',  ( -69.75874677887840392, -25.29662546892861386, 5.475966365782060308 ) ) ;
#78198=FACE_OUTER_BOUND ( 'NONE', #85776, .T. ) ;
#78199=CARTESIAN_POINT ( 'NONE',  ( -89.49044894935767047, -25.12049752546738191, 2.832404795212222659 ) ) ;
#78201=CARTESIAN_POINT ( 'NONE',  ( 19.27460657395150889, -5.330843762518559181, -1.500000000000002220 ) ) ;
#78203=FACE_OUTER_BOUND ( 'NONE', #36312, .T. ) ;
#78207=AXIS2_PLACEMENT_3D ( 'NONE', #32259, #72337, #40379 ) ;
#78210=CARTESIAN_POINT ( 'NONE',  ( -79.64684267427536213, -23.48786465467241058, 11.44779295918254824 ) ) ;
#78211=CARTESIAN_POINT ( 'NONE',  ( -110.3009842343709721, -25.18430154008630595, 3.294836824253255081 ) ) ;
#78212=CARTESIAN_POINT ( 'NONE',  ( -35.49723519497781865, -24.15503026093914940, -0.2815557561904327155 ) ) ;
#78214=CARTESIAN_POINT ( 'NONE',  ( -118.3656671591979261, -25.31826104724058979, 3.540018580561490324 ) ) ;
#78216=DIRECTION ( 'NONE',  ( 3.773278334444166432E-23, -1.000000000000000000, 0.000000000000000000 ) ) ;
#78217=AXIS2_PLACEMENT_3D ( 'NONE', #15058, #40409, #8454 ) ;
#78218=CARTESIAN_POINT ( 'NONE',  ( -90.62287095715004170, -29.50250786944525672, 11.44777988621623344 ) ) ;
#78219=ORIENTED_EDGE ( 'NONE', *, *, #92533, .F. ) ;
#78220=CARTESIAN_POINT ( 'NONE',  ( 20.23688964843749005, 1.552196809742036221, 11.49999999999998934 ) ) ;
#78223=CARTESIAN_POINT ( 'NONE',  ( -88.52287095715006160, -23.48786465467241769, 11.44779295918254292 ) ) ;
#78224=ORIENTED_EDGE ( 'NONE', *, *, #71798, .F. ) ;
#78225=DIRECTION ( 'NONE',  ( 3.773278334444167608E-23, -1.000000000000000000, 0.000000000000000000 ) ) ;
#78226=CARTESIAN_POINT ( 'NONE',  ( 5.670567493371958534, -19.34269084982597775, -1.500000000000002220 ) ) ;
#78227=CARTESIAN_POINT ( 'NONE',  ( -9.089321149825819290, -19.05894737874082168, 11.49999999999999645 ) ) ;
#78228=CARTESIAN_POINT ( 'NONE',  ( 22.02032638543937182, 1.892999326154024553, 11.49999999999998934 ) ) ;
#78229=CARTESIAN_POINT ( 'NONE',  ( 9.245221688665949955, -18.36014492602614467, -1.500000000000002220 ) ) ;
#78231=ORIENTED_EDGE ( 'NONE', *, *, #58731, .T. ) ;
#78232=DIRECTION ( 'NONE',  ( 0.000000000000000000, -0.9999999999976377785, -2.173523156925979128E-06 ) ) ;
#78233=EDGE_LOOP ( 'NONE', ( #34573, #28503, #63459, #97158 ) ) ;
#78235=CARTESIAN_POINT ( 'NONE',  ( -110.6228709571501128, -24.83620972994592080, 8.398175272781363887 ) ) ;
#78236=ORIENTED_EDGE ( 'NONE', *, *, #49163, .T. ) ;
#78237=ORIENTED_EDGE ( 'NONE', *, *, #88865, .F. ) ;
#78238=B_SPLINE_CURVE_WITH_KNOTS ( 'NONE', 3,
 ( #47737, #77659, #93897, #549 ),
 .UNSPECIFIED., .F., .F.,
 ( 4, 4 ),
 ( 0.2389318754978128900, 0.2399326225385782496 ),
 .UNSPECIFIED. ) ;
#78239=ORIENTED_EDGE ( 'NONE', *, *, #82637, .F. ) ;
#78241=CARTESIAN_POINT ( 'NONE',  ( -55.62287095715004170, -24.99156045073392463, 7.747789690856161648 ) ) ;
#78243=CARTESIAN_POINT ( 'NONE',  ( -14.43086120294938368, -14.79396848081076854, -1.500000000000002220 ) ) ;
#78244=CARTESIAN_POINT ( 'NONE',  ( 16.98214085172422827, 13.50221961261776293, 11.49999999999999645 ) ) ;
#78245=ORIENTED_EDGE ( 'NONE', *, *, #36830, .F. ) ;
#78247=CARTESIAN_POINT ( 'NONE',  ( -41.62287095715006302, -23.47596703998600276, 11.44779298504227505 ) ) ;
#78249=CARTESIAN_POINT ( 'NONE',  ( 3.752539591237177508, -22.04708138622333635, 11.49999999999998934 ) ) ;
#78250=CARTESIAN_POINT ( 'NONE',  ( -47.58188357232938159, -24.51419770103156637, 9.386484678747176957 ) ) ;
#78251=CARTESIAN_POINT ( 'NONE',  ( -101.5228709571500758, -24.64965694238407323, 8.947790433994194714 ) ) ;
#78252=EDGE_LOOP ( 'NONE', ( #92259, #59594, #2476, #32368 ) ) ;
#78253=CARTESIAN_POINT ( 'NONE',  ( -117.2170119873909329, -25.33573473601760995, 6.311387531435581622 ) ) ;
#78254=CARTESIAN_POINT ( 'NONE',  ( -35.48359714022421940, -24.52399227489126687, 9.353111116836519301 ) ) ;
#78257=CARTESIAN_POINT ( 'NONE',  ( -110.5228709571500616, -23.47596703998600631, 11.44779298504228038 ) ) ;
#78259=FACE_OUTER_BOUND ( 'NONE', #77526, .T. ) ;
#78260=CARTESIAN_POINT ( 'NONE',  ( -20.81765089029956783, 3.879123387127271005, -1.500000000000002220 ) ) ;
#78261=ORIENTED_EDGE ( 'NONE', *, *, #93067, .F. ) ;
#78263=ADVANCED_FACE ( 'NONE', ( #65524 ), #57901, .F. ) ;
#78264=CARTESIAN_POINT ( 'NONE',  ( -20.57666286913221754, 7.287794730890116313, 11.49999999999998934 ) ) ;
#78265=PLANE ( 'NONE',  #75625 ) ;
#78266=ADVANCED_FACE ( 'NONE', ( #21298 ), #85592, .T. ) ;
#78267=FACE_OUTER_BOUND ( 'NONE', #88344, .T. ) ;
#78269=CARTESIAN_POINT ( 'NONE',  ( -18.25314811174894913, -11.95880190493418738, -1.500000000000002220 ) ) ;
#78270=CARTESIAN_POINT ( 'NONE',  ( -30.57287095715005520, -23.78465599299007849, 10.96065251130191776 ) ) ;
#78273=CARTESIAN_POINT ( 'NONE',  ( -85.64374319538433156, -23.85049219812685450, 10.88485053497527133 ) ) ;
#78274=VERTEX_POINT ( 'NONE', #75089 ) ;
#78275=ADVANCED_FACE ( 'NONE', ( #44156 ), #2560, .F. ) ;
#78277=ORIENTED_EDGE ( 'NONE', *, *, #61054, .T. ) ;
#78278=EDGE_CURVE ( 'NONE', #26092, #27769, #16691, .T. ) ;
#78279=AXIS2_PLACEMENT_3D ( 'NONE', #26441, #4605, #35553 ) ;
#78280=B_SPLINE_CURVE_WITH_KNOTS ( 'NONE', 3,
 ( #97080, #20941, #44305, #20440 ),
 .UNSPECIFIED., .F., .F.,
 ( 4, 4 ),
 ( 0.000000000000000000, 9.999999999997510880E-05 ),
 .UNSPECIFIED. ) ;
#78281=ORIENTED_EDGE ( 'NONE', *, *, #77008, .F. ) ;
#78284=CARTESIAN_POINT ( 'NONE',  ( -82.55076503047374104, -24.15543982623907482, -0.2315651400026498552 ) ) ;
#78285=CARTESIAN_POINT ( 'NONE',  ( -17.82860346875387947, 11.52481846644873187, -1.500000000000002220 ) ) ;
#78286=B_SPLINE_CURVE_WITH_KNOTS ( 'NONE', 3,
 ( #83442, #100140, #13432, #36784 ),
 .UNSPECIFIED., .F., .F.,
 ( 4, 4 ),
 ( 0.000000000000000000, 0.0001002978982766898939 ),
 .UNSPECIFIED. ) ;
#78287=CARTESIAN_POINT ( 'NONE',  ( -94.58429178781234725, -24.65952944569304606, 1.056160979905703234 ) ) ;
#78288=CARTESIAN_POINT ( 'NONE',  ( -30.62155233649868791, -24.14929313691197521, 10.49653219292474482 ) ) ;
#78290=DIRECTION ( 'NONE',  ( -1.000000000000000000, -3.773278334444166432E-23, -8.201307841325785021E-29 ) ) ;
#78291=AXIS2_PLACEMENT_3D ( 'NONE', #84542, #7416, #59731 ) ;
#78292=CARTESIAN_POINT ( 'NONE',  ( 4.312616920666290987, -18.91975033782923887, 11.49999999999998934 ) ) ;
#78293=CARTESIAN_POINT ( 'NONE',  ( -40.93200155000062068, -25.32724636324323342, 4.398074533285874388 ) ) ;
#78294=ORIENTED_EDGE ( 'NONE', *, *, #91912, .T. ) ;
#78295=CARTESIAN_POINT ( 'NONE',  ( 1.793504005174451077, 19.40006364325761012, 11.49999999999999645 ) ) ;
#78298=CARTESIAN_POINT ( 'NONE',  ( -79.62463646828913966, -25.18409543558836816, 6.717720826779347121 ) ) ;
#78302=CARTESIAN_POINT ( 'NONE',  ( -59.52287095715006870, -23.96177878511308990, 10.65340807706329862 ) ) ;
#78303=CARTESIAN_POINT ( 'NONE',  ( -30.53953689203329702, -23.47593904782709018, -1.430909884246568842 ) ) ;
#78304=CARTESIAN_POINT ( 'NONE',  ( -93.63080997736221889, -24.15620529776628445, 10.23563542870659404 ) ) ;
#78305=CARTESIAN_POINT ( 'NONE',  ( 0.7808950796103379943, -19.64173473864696717, -1.500000000000002220 ) ) ;
#78307=B_SPLINE_SURFACE_WITH_KNOTS ( 'NONE', 3, 3, ( 
 ( #39620, #72588, #34019, #8680 ),
 ( #62984, #47747, #36006, #58854 ),
 ( #89304, #88811, #26405, #65994 ),
 ( #11666, #96912, #4575, #73581 ),
 ( #73089, #18779, #97409, #27406 ),
 ( #19277, #27898, #20766, #58365 ),
 ( #95912, #59349, #35020, #75055 ) ),
 .UNSPECIFIED., .F., .F., .F.,
 ( 4, 3, 4 ),
 ( 4, 4 ),
 ( 0.7945040050992236980, 0.8970133687736498995, 0.9995227324480762121 ),
 ( 0.6596616264046517575, 0.6609788945409680316 ),
 .UNSPECIFIED. ) ;
#78308=CARTESIAN_POINT ( 'NONE',  ( -41.34727404100192416, -25.31583668745965809, 4.610738936032308111 ) ) ;
#78310=CARTESIAN_POINT ( 'NONE',  ( 18.62697458635512859, 10.92912097662538251, 11.49999999999998934 ) ) ;
#78313=CARTESIAN_POINT ( 'NONE',  ( -5.338719972479099241, 22.46511350730333589, -1.500000000000002220 ) ) ;
#78315=FACE_OUTER_BOUND ( 'NONE', #2510, .T. ) ;
#78317=FACE_OUTER_BOUND ( 'NONE', #12711, .T. ) ;
#78318=CARTESIAN_POINT ( 'NONE',  ( -64.62287095715005592, -24.35013146730203459, 9.818937971375113705 ) ) ;
#78319=CARTESIAN_POINT ( 'NONE',  ( -111.7494854843401555, -25.29824069328104486, 4.020187583360979922 ) ) ;
#78320=CARTESIAN_POINT ( 'NONE',  ( -121.6228709571500843, -23.96177878511308990, 10.65340807706329862 ) ) ;
#78321=CARTESIAN_POINT ( 'NONE',  ( -114.5892327960407187, -24.35071581493544102, 9.817618358456016381 ) ) ;
#78322=CARTESIAN_POINT ( 'NONE',  ( -7.573260116017839216, 18.43532004384545786, 11.49999999999998934 ) ) ;
#78324=PLANE ( 'NONE',  #87290 ) ;
#78325=CARTESIAN_POINT ( 'NONE',  ( 1.944447714513537262, -19.71154682592685958, -1.500000000000002220 ) ) ;
#78326=CARTESIAN_POINT ( 'NONE',  ( -56.65018345228885011, -23.73766607897670511, -1.055555164236459342 ) ) ;
#78327=EDGE_CURVE ( 'NONE', #6143, #50179, #63905, .T. ) ;
#78328=VECTOR ( 'NONE', #43506, 1000.000000000000114 ) ;
#78329=CARTESIAN_POINT ( 'NONE',  ( -93.52287095715006160, -23.47593901973090524, -1.443836447538996648 ) ) ;
#78330=CARTESIAN_POINT ( 'NONE',  ( -99.64934318012689118, -25.30535455722350591, 4.927356316503054501 ) ) ;
#78331=CARTESIAN_POINT ( 'NONE',  ( -8.119355292522030254, -19.11072509857415369, 11.49999999999999645 ) ) ;
#78332=CARTESIAN_POINT ( 'NONE',  ( -101.9228709571500815, -23.47596703998600631, 11.44779298504227683 ) ) ;
#78333=EDGE_CURVE ( 'NONE', #66467, #92752, #89173, .T. ) ;
#78334=DIRECTION ( 'NONE',  ( 0.000000000000000000, -2.173523156925979552E-06, 0.9999999999976378895 ) ) ;
#78335=CARTESIAN_POINT ( 'NONE',  ( -17.61067154241388977, 14.45706175128816184, 11.49999999999999645 ) ) ;
#78336=VERTEX_POINT ( 'NONE', #41044 ) ;
#78337=CARTESIAN_POINT ( 'NONE',  ( -83.62287095715011276, -23.96177878511308634, 10.65340807706329684 ) ) ;
#78338=CARTESIAN_POINT ( 'NONE',  ( -106.6228709571500275, -23.72747288104469732, -1.053458166803225016 ) ) ;
#78339=ORIENTED_EDGE ( 'NONE', *, *, #18627, .T. ) ;
#78340=CARTESIAN_POINT ( 'NONE',  ( 17.48260522047220888, -10.12088315688240314, -1.500000000000002220 ) ) ;
#78341=B_SPLINE_CURVE_WITH_KNOTS ( 'NONE', 3,
 ( #44424, #13948, #68251, #64156, #2243, #8840 ),
 .UNSPECIFIED., .F., .F.,
 ( 4, 2, 4 ),
 ( 0.000000000000000000, 0.001380764517854766267, 0.002761529035709532533 ),
 .UNSPECIFIED. ) ;
#78343=AXIS2_PLACEMENT_3D ( 'NONE', #98709, #49317, #61670 ) ;
#78344=CARTESIAN_POINT ( 'NONE',  ( -41.31743941260997133, -25.30152573394828863, 4.668812341817115907 ) ) ;
#78345=ORIENTED_EDGE ( 'NONE', *, *, #56986, .T. ) ;
#78346=CARTESIAN_POINT ( 'NONE',  ( -70.62287095715008434, -23.84081130438201157, 10.88220057463249013 ) ) ;
#78347=CARTESIAN_POINT ( 'NONE',  ( -19.87571804785047647, -11.42512898079034400, 11.49999999999998934 ) ) ;
#78348=CARTESIAN_POINT ( 'NONE',  ( -41.86664830098052192, -25.28370616383384828, 4.117318242077936397 ) ) ;
#78349=CARTESIAN_POINT ( 'NONE',  ( -21.62496174240652991, 0.2022338437372764308, -1.500000000000002220 ) ) ;
#78350=CARTESIAN_POINT ( 'NONE',  ( -41.05437968932909598, -25.04895513844916266, 7.488404314379859983 ) ) ;
#78351=CARTESIAN_POINT ( 'NONE',  ( 0.7041596644206948863, -20.94928778062849162, 11.49999999999999645 ) ) ;
#78354=CARTESIAN_POINT ( 'NONE',  ( -124.5899959654626770, -24.15543982623907127, -0.2315651400026562945 ) ) ;
#78355=CARTESIAN_POINT ( 'NONE',  ( -11.61111146657235871, -18.70866699758865792, 11.49999999999998934 ) ) ;
#78357=AXIS2_PLACEMENT_3D ( 'NONE', #96422, #82185, #43634 ) ;
#78360=CARTESIAN_POINT ( 'NONE',  ( -126.5228709571500616, -29.50248528299804818, 1.056150453629047137 ) ) ;
#78361=ORIENTED_EDGE ( 'NONE', *, *, #10198, .F. ) ;
#78363=ORIENTED_EDGE ( 'NONE', *, *, #59043, .F. ) ;
#78368=CARTESIAN_POINT ( 'NONE',  ( -36.59394419572883095, -24.15543982623907127, -0.2315651400026672579 ) ) ;
#78369=B_SPLINE_CURVE_WITH_KNOTS ( 'NONE', 3,
 ( #36901, #12564, #83056, #74464, #60256, #4957 ),
 .UNSPECIFIED., .F., .F.,
 ( 4, 2, 4 ),
 ( 6.384118678618877625E-06, 0.001386860460828382140, 0.002767336802978145362 ),
 .UNSPECIFIED. ) ;
#78370=CARTESIAN_POINT ( 'NONE',  ( 5.028806042385554953, -19.83023610923392610, -1.500000000000002220 ) ) ;
#78372=CARTESIAN_POINT ( 'NONE',  ( -99.52232038167861106, -25.29196717039579312, 5.580301540147455164 ) ) ;
#78373=CARTESIAN_POINT ( 'NONE',  ( -44.58162010085130333, -24.51314013834316086, 0.6176544820404110681 ) ) ;
#78374=CARTESIAN_POINT ( 'NONE',  ( -43.62287095715004881, -29.50250786944525672, 11.44777988621624232 ) ) ;
#78375=CARTESIAN_POINT ( 'NONE',  ( 22.30035941410032763, -0.3387204123245128873, -1.500000000000002220 ) ) ;
#78376=CARTESIAN_POINT ( 'NONE',  ( -0.1490749075164066184, -21.12010817310450861, 11.44779298504228038 ) ) ;
#78380=CARTESIAN_POINT ( 'NONE',  ( -118.5228709571500900, -24.50216790748206108, 0.6166512839542579449 ) ) ;
#78381=CARTESIAN_POINT ( 'NONE',  ( -18.77111393065419875, 9.022841878967760465, 11.49999999999998934 ) ) ;
#78382=ORIENTED_EDGE ( 'NONE', *, *, #94550, .T. ) ;
#78383=CARTESIAN_POINT ( 'NONE',  ( -122.6228709571500417, -29.50247984919015209, -1.443849546365046699 ) ) ;
#78384=ORIENTED_EDGE ( 'NONE', *, *, #37532, .T. ) ;
#78385=B_SPLINE_CURVE_WITH_KNOTS ( 'NONE', 3,
 ( #76376, #59184, #53073, #22578 ),
 .UNSPECIFIED., .F., .F.,
 ( 4, 4 ),
 ( 0.3000001472394721591, 0.3090065785115879704 ),
 .UNSPECIFIED. ) ;
#78386=EDGE_LOOP ( 'NONE', ( #96232, #26248, #82367, #59885 ) ) ;
#78387=EDGE_CURVE ( 'NONE', #67625, #30682, #4347, .T. ) ;
#78388=CARTESIAN_POINT ( 'NONE',  ( -50.45832920465950622, -25.25854569161092300, 7.100425421451603825 ) ) ;
#78389=CARTESIAN_POINT ( 'NONE',  ( -20.81348254183067681, -2.960215062046979373, -1.500000000000002220 ) ) ;
#78390=ORIENTED_EDGE ( 'NONE', *, *, #93611, .T. ) ;
#78395=CARTESIAN_POINT ( 'NONE',  ( -101.1119640259560271, -25.25419526093012479, 7.433727736561444921 ) ) ;
#78396=CARTESIAN_POINT ( 'NONE',  ( -60.62287095715004881, -23.84081130438200802, 10.88220057463249013 ) ) ;
#78397=CARTESIAN_POINT ( 'NONE',  ( -117.9228709571500673, -23.47596703998600276, 11.44779298504227683 ) ) ;
#78398=CARTESIAN_POINT ( 'NONE',  ( -21.14524153552446606, 6.695245452574716261, 11.49999999999999645 ) ) ;
#78399=ORIENTED_EDGE ( 'NONE', *, *, #2703, .T. ) ;
#78400=CARTESIAN_POINT ( 'NONE',  ( -88.88918693012689687, -25.26877915520014639, 5.947789088310639904 ) ) ;
#78401=CARTESIAN_POINT ( 'NONE',  ( -105.5228709571500758, -23.47596703998600631, 11.44779298504228038 ) ) ;
#78403=VECTOR ( 'NONE', #89231, 1000.000000000000114 ) ;
#78405=CARTESIAN_POINT ( 'NONE',  ( -18.74212433040710479, 12.77821124017617649, -1.500000000000002220 ) ) ;
#78406=ADVANCED_FACE ( 'NONE', ( #80096 ), #11086, .F. ) ;
#78409=B_SPLINE_CURVE_WITH_KNOTS ( 'NONE', 3,
 ( #54148, #31795, #53646, #55142, #86575, #100271, #15556, #46518 ),
 .UNSPECIFIED., .F., .F.,
 ( 4, 2, 2, 4 ),
 ( 6.391158118964588215E-06, 0.002007136338672922248, 0.003007508928949903428, 0.004007881519226885042 ),
 .UNSPECIFIED. ) ;
#78413=ADVANCED_FACE ( 'NONE', ( #35432 ), #19681, .F. ) ;
#78415=CARTESIAN_POINT ( 'NONE',  ( 2.654622155064554789, -19.98241913370796041, -1.500000000000002220 ) ) ;
#78417=VERTEX_POINT ( 'NONE', #82096 ) ;
#78418=LINE ( 'NONE', #23122, #97359 ) ;
#78419=CARTESIAN_POINT ( 'NONE',  ( -19.80502325505778671, 10.42642913751328670, -1.500000000000002220 ) ) ;
#78420=ORIENTED_EDGE ( 'NONE', *, *, #4536, .T. ) ;
#78421=ORIENTED_EDGE ( 'NONE', *, *, #76958, .F. ) ;
#78422=CARTESIAN_POINT ( 'NONE',  ( -34.52287095715006160, -23.72773821059536203, 11.05748984161097326 ) ) ;
#78423=CARTESIAN_POINT ( 'NONE',  ( -94.62356963122135767, -24.66019654487199730, 8.947790411086121054 ) ) ;
#78426=CARTESIAN_POINT ( 'NONE',  ( -63.93325875615660436, -24.26743686635980879, 0.04347934593174120760 ) ) ;
#78427=CARTESIAN_POINT ( 'NONE',  ( -2.459534284235005863, 19.42625828800391119, 11.49999999999998934 ) ) ;
#78429=ORIENTED_EDGE ( 'NONE', *, *, #93007, .T. ) ;
#78430=CARTESIAN_POINT ( 'NONE',  ( 12.90647603486358364, 17.18646895862681134, 11.49999999999998934 ) ) ;
#78431=CARTESIAN_POINT ( 'NONE',  ( -36.58953762381672448, -23.47593901973091235, -1.443836447539011525 ) ) ;
#78433=DIRECTION ( 'NONE',  ( -3.773278334444166432E-23, 1.000000000000000000, 0.000000000000000000 ) ) ;
#78435=CARTESIAN_POINT ( 'NONE',  ( 9.743704349311032686, 20.77413290702584092, -1.500000000000002220 ) ) ;
#78437=CARTESIAN_POINT ( 'NONE',  ( -120.5562042904834072, -25.00158670708909625, 2.256160236439166411 ) ) ;
#78438=CARTESIAN_POINT ( 'NONE',  ( -70.41995703322675126, -25.31157400179870720, 5.314953636079311927 ) ) ;
#78439=CARTESIAN_POINT ( 'NONE',  ( 15.84714387567644955, -12.28532832577633194, 11.49999999999999645 ) ) ;
#78440=CARTESIAN_POINT ( 'NONE',  ( -79.24831702480813078, -25.26612486446449779, 5.024332913579260484 ) ) ;
#78441=CARTESIAN_POINT ( 'NONE',  ( -57.62287095715004881, -24.66019654487199020, 8.947790411086131712 ) ) ;
#78445=LINE ( 'NONE', #32784, #88303 ) ;
#78446=CARTESIAN_POINT ( 'NONE',  ( -9.430186865587145917, -19.61854929170128869, 11.49999999999998934 ) ) ;
#78448=CARTESIAN_POINT ( 'NONE',  ( -15.16924259816527609, 12.53091941037558854, -1.500000000000002220 ) ) ;
#78450=CARTESIAN_POINT ( 'NONE',  ( -109.3951644950792996, -25.27925728710133413, 4.495754977740414660 ) ) ;
#78452=CARTESIAN_POINT ( 'NONE',  ( -91.55469187719226909, -23.96169478059713498, 10.65365249895718058 ) ) ;
#78454=CARTESIAN_POINT ( 'NONE',  ( 20.20254288951482735, -3.758238384022974277, 11.49999999999999645 ) ) ;
#78456=EDGE_CURVE ( 'NONE', #43726, #22752, #6842, .T. ) ;
#78457=AXIS2_PLACEMENT_3D ( 'NONE', #49904, #80838, #36652 ) ;
#78458=CARTESIAN_POINT ( 'NONE',  ( -120.5222358249351799, -23.48783264082477018, -1.443836473390085695 ) ) ;
#78459=CARTESIAN_POINT ( 'NONE',  ( -17.13258802378025791, -14.77425600068537115, 11.49999999999999645 ) ) ;
#78460=ORIENTED_EDGE ( 'NONE', *, *, #76885, .F. ) ;
#78462=CARTESIAN_POINT ( 'NONE',  ( -83.58953762381672448, -23.47596703998600276, 11.44779298504227683 ) ) ;
#78464=CARTESIAN_POINT ( 'NONE',  ( -74.52287095715007581, -24.64965694238408034, 8.947790433994200043 ) ) ;
#78466=CARTESIAN_POINT ( 'NONE',  ( -49.52287095715006160, -29.50248528299804818, 1.056150453629033370 ) ) ;
#78470=CARTESIAN_POINT ( 'NONE',  ( 13.31140876108729998, -18.89465134148960956, 11.49999999999999645 ) ) ;
#78471=CARTESIAN_POINT ( 'NONE',  ( 20.53691900564983186, 10.01969956684014207, 11.49999999999998934 ) ) ;
#78472=CARTESIAN_POINT ( 'NONE',  ( -74.54209746499468281, -24.51314013834315375, 0.6176544820404125113 ) ) ;
#78473=CARTESIAN_POINT ( 'NONE',  ( -96.55228966665733026, -24.15543982623907482, -0.2315651400026596807 ) ) ;
#78474=CARTESIAN_POINT ( 'NONE',  ( -82.60435760244244818, -23.48786465467241058, 11.44779295918254647 ) ) ;
#78475=CARTESIAN_POINT ( 'NONE',  ( -1.649324495273077451, -22.40575143947253167, 11.49999999999999645 ) ) ;
#78476=ORIENTED_EDGE ( 'NONE', *, *, #32591, .F. ) ;
#78477=CARTESIAN_POINT ( 'NONE',  ( -43.51356542795910798, -23.73766607897671221, -1.055555164236442689 ) ) ;
#78478=CARTESIAN_POINT ( 'NONE',  ( 21.83198049998918577, 2.282343850347359648, 11.49999999999998934 ) ) ;
#78480=EDGE_CURVE ( 'NONE', #52307, #77573, #28590, .T. ) ;
#78482=CARTESIAN_POINT ( 'NONE',  ( -34.48363162486440103, -24.51419770103156637, 9.386484678747176957 ) ) ;
#78484=VERTEX_POINT ( 'NONE', #49171 ) ;
#78485=CARTESIAN_POINT ( 'NONE',  ( -48.50690933534888671, -23.96169478059713143, 10.65365249895718236 ) ) ;
#78487=ORIENTED_EDGE ( 'NONE', *, *, #1202, .T. ) ;
#78488=CARTESIAN_POINT ( 'NONE',  ( -16.05948562299510485, -12.68841425896798469, -1.500000000000002220 ) ) ;
#78491=EDGE_LOOP ( 'NONE', ( #63460, #75622, #39255, #4549 ) ) ;
#78493=CARTESIAN_POINT ( 'NONE',  ( -5.126879528927636542, -22.49243673399587351, 11.49999999999998934 ) ) ;
#78494=CARTESIAN_POINT ( 'NONE',  ( -50.22074830152320146, -25.12160478917137141, 2.838478583573862846 ) ) ;
#78495=CARTESIAN_POINT ( 'NONE',  ( -12.33117494125061242, 16.09929768045241261, -1.500000000000002220 ) ) ;
#78498=CARTESIAN_POINT ( 'NONE',  ( -37.52287095715008292, -23.48783264083359512, -1.443836473376374885 ) ) ;
#78499=CARTESIAN_POINT ( 'NONE',  ( -37.62287095715005592, -29.50247984919015209, -1.443849546365060466 ) ) ;
#78500=CARTESIAN_POINT ( 'NONE',  ( -98.52287095715006160, -23.47596703998600631, 11.44779298504228215 ) ) ;
#78501=CARTESIAN_POINT ( 'NONE',  ( 21.22668844964908885, 3.412186807495566132, 11.49999999999999645 ) ) ;
#78503=CARTESIAN_POINT ( 'NONE',  ( -89.58953762381671027, -24.64965694238407323, 8.947790433994651238 ) ) ;
#78505=ORIENTED_EDGE ( 'NONE', *, *, #27924, .T. ) ;
#78506=CARTESIAN_POINT ( 'NONE',  ( 20.74337371777590278, 0.4424840333690017724, -1.500000000000002220 ) ) ;
#78507=ORIENTED_EDGE ( 'NONE', *, *, #31541, .F. ) ;
#78508=CARTESIAN_POINT ( 'NONE',  ( -125.5892687586139260, -24.73486907724918638, 1.287355809206972346 ) ) ;
#78509=ORIENTED_EDGE ( 'NONE', *, *, #32587, .F. ) ;
#78510=CARTESIAN_POINT ( 'NONE',  ( -111.5222191119067645, -23.48786465467241769, 11.44779295918254114 ) ) ;
#78513=ORIENTED_EDGE ( 'NONE', *, *, #79093, .T. ) ;
#78514=PLANE ( 'NONE',  #98018 ) ;
#78515=CARTESIAN_POINT ( 'NONE',  ( -83.62287095715005592, -29.50248528299804818, 1.056150453629038477 ) ) ;
#78516=CARTESIAN_POINT ( 'NONE',  ( -28.42914491461137061, -24.71144043923981215, 1.770770211163098296 ) ) ;
#78517=CARTESIAN_POINT ( 'NONE',  ( -17.76638496452178018, -13.01238552544781335, 11.49999999999999645 ) ) ;
#78519=CARTESIAN_POINT ( 'NONE',  ( 2.010693963185784749, 22.50221635003889276, 11.49999999999998934 ) ) ;
#78520=CARTESIAN_POINT ( 'NONE',  ( 17.27681320446407298, 11.92757687370068886, -1.500000000000002220 ) ) ;
#78522=CARTESIAN_POINT ( 'NONE',  ( -70.62287095715005592, -24.99132157543083821, 2.256160258750667502 ) ) ;
#78527=CARTESIAN_POINT ( 'NONE',  ( -59.62287095715007723, -23.47596703998600276, 11.44779298504227683 ) ) ;
#78529=CARTESIAN_POINT ( 'NONE',  ( -114.5228709571500758, -23.47593901973090524, -1.443836447538996204 ) ) ;
#78530=ORIENTED_EDGE ( 'NONE', *, *, #1879, .F. ) ;
#78531=CARTESIAN_POINT ( 'NONE',  ( 19.19679251752027227, 8.867671107084703408, -1.500000000000002220 ) ) ;
#78532=DIRECTION ( 'NONE',  ( 0.000000000000000000, -0.9999999999976377785, -2.173523156925979128E-06 ) ) ;
#78533=CARTESIAN_POINT ( 'NONE',  ( -50.91781549829847364, -25.03148729399882200, 7.505037586422455220 ) ) ;
#78534=CARTESIAN_POINT ( 'NONE',  ( -121.5888804960365377, -24.51314013834316441, 0.6176544820404217262 ) ) ;
#78537=CARTESIAN_POINT ( 'NONE',  ( 8.998109643811913472, -20.30750954041392120, -1.500000000000002220 ) ) ;
#78538=CARTESIAN_POINT ( 'NONE',  ( -49.44333826525905806, -25.03220847003835559, 7.288210503460494039 ) ) ;
#78539=EDGE_CURVE ( 'NONE', #12627, #12501, #50652, .T. ) ;
#78543=CARTESIAN_POINT ( 'NONE',  ( -37.60092958079493997, -23.96119346886880663, -0.6495511937831990323 ) ) ;
#78545=CARTESIAN_POINT ( 'NONE',  ( -100.6266800081263284, -24.73486907724917572, 1.287355809206965240 ) ) ;
#78546=CARTESIAN_POINT ( 'NONE',  ( -100.6000550215268845, -25.11144175452923477, 2.838473218577969082 ) ) ;
#78547=CARTESIAN_POINT ( 'NONE',  ( 17.91360334016800593, 7.682165803940314674, 11.49999999999998934 ) ) ;
#78548=CARTESIAN_POINT ( 'NONE',  ( -20.93543047832761417, 4.563121699532205255, 11.49999999999998934 ) ) ;
#78549=CARTESIAN_POINT ( 'NONE',  ( -89.52287095715006160, -29.50248528299804818, 1.056150453629040253 ) ) ;
#78551=FACE_OUTER_BOUND ( 'NONE', #45501, .T. ) ;
#78552=CARTESIAN_POINT ( 'NONE',  ( -101.0406423489954477, -25.18440054762538693, 3.494480559635227301 ) ) ;
#78553=CARTESIAN_POINT ( 'NONE',  ( 20.46598465274837864, -9.837531852206524263, -1.500000000000002220 ) ) ;
#78554=CARTESIAN_POINT ( 'NONE',  ( -106.5562042904834215, -23.47593901973091235, -1.443836447538999312 ) ) ;
#78556=CARTESIAN_POINT ( 'NONE',  ( -9.893332137849947472, -17.22304987741864579, 11.49999999999999645 ) ) ;
#78557=CARTESIAN_POINT ( 'NONE',  ( -123.5209511861243072, -23.96169478059714564, 10.65365249895717170 ) ) ;
#78558=CARTESIAN_POINT ( 'NONE',  ( -60.95156673781919920, -25.20074414427590526, 3.409327697718777195 ) ) ;
#78560=ORIENTED_EDGE ( 'NONE', *, *, #41424, .F. ) ;
#78561=CARTESIAN_POINT ( 'NONE',  ( -49.27764846858840997, -25.25176233969420636, 6.145204990682164414 ) ) ;
#78564=CARTESIAN_POINT ( 'NONE',  ( -14.16021466491576675, 16.42052772630311352, -1.500000000000002220 ) ) ;
#78565=CARTESIAN_POINT ( 'NONE',  ( -115.5228709571500758, -25.00182538069145721, 7.747789668545101094 ) ) ;
#78566=CARTESIAN_POINT ( 'NONE',  ( 4.731349760756693890, 18.90081699332259646, -1.500000000000002220 ) ) ;
#78567=CARTESIAN_POINT ( 'NONE',  ( -55.63149466436955493, -24.73531770709094957, 8.716586749053510275 ) ) ;
#78568=EDGE_CURVE ( 'NONE', #62952, #92846, #24996, .T. ) ;
#78569=ORIENTED_EDGE ( 'NONE', *, *, #69765, .T. ) ;
#78571=CARTESIAN_POINT ( 'NONE',  ( 2.554409723529738052, 20.22502395925995700, 11.49999999999999645 ) ) ;
#78572=CARTESIAN_POINT ( 'NONE',  ( -84.62287095715005592, -29.50247984919015209, -1.443849546365053582 ) ) ;
#78574=CARTESIAN_POINT ( 'NONE',  ( -107.6228709571500701, -29.50250786944525672, 11.44777988621622988 ) ) ;
#78575=VERTEX_POINT ( 'NONE', #96323 ) ;
#78578=CARTESIAN_POINT ( 'NONE',  ( -39.42702772597635175, -25.27985508946863291, 5.331662265757392660 ) ) ;
#78579=CARTESIAN_POINT ( 'NONE',  ( -40.58885790174546315, -24.52399227489126687, 9.353111116836521077 ) ) ;
#78581=CARTESIAN_POINT ( 'NONE',  ( 10.48293302797296356, 17.13603372422173976, -1.500000000000002220 ) ) ;
#78584=CARTESIAN_POINT ( 'NONE',  ( -66.63133170827177310, -24.35071581493543036, 9.817618358456028815 ) ) ;
#78585=CARTESIAN_POINT ( 'NONE',  ( -3.094460115123966570, -22.75893099265358188, 11.49999999999999645 ) ) ;
#78586=CARTESIAN_POINT ( 'NONE',  ( 11.07647423179810531, -19.82844882884714366, -1.500000000000002220 ) ) ;
#78589=CARTESIAN_POINT ( 'NONE',  ( -91.62287095715005592, -23.48786465467241769, 11.44779295918254114 ) ) ;
#78590=CARTESIAN_POINT ( 'NONE',  ( -38.49109438492880741, -24.35071581493542325, 9.817618358456030592 ) ) ;
#78592=VECTOR ( 'NONE', #41440, 1000.000000000000114 ) ;
#78594=CARTESIAN_POINT ( 'NONE',  ( -128.5898162796150075, -24.15620529776629510, 10.23563542870659404 ) ) ;
#78595=CARTESIAN_POINT ( 'NONE',  ( -26.19597845478084608, -24.90840837394421570, 3.802218847965264992 ) ) ;
#78597=CARTESIAN_POINT ( 'NONE',  ( -98.92944106970213625, -25.25460656324785447, 5.790834282400935784 ) ) ;
#78598=ORIENTED_EDGE ( 'NONE', *, *, #77992, .T. ) ;
#78599=CARTESIAN_POINT ( 'NONE',  ( -13.40315722217803973, 15.35114911505495172, 11.49999999999998934 ) ) ;
#78600=ORIENTED_EDGE ( 'NONE', *, *, #71737, .F. ) ;
#78601=CARTESIAN_POINT ( 'NONE',  ( -22.63010559926462051, 4.001702944626347680, -1.500000000000002220 ) ) ;
#78603=VECTOR ( 'NONE', #98744, 1000.000000000000114 ) ;
#78607=CARTESIAN_POINT ( 'NONE',  ( -35.52287095715008292, -25.00182538069144655, 7.747789668545105535 ) ) ;
#78609=B_SPLINE_CURVE_WITH_KNOTS ( 'NONE', 3,
 ( #42912, #81959, #74347, #2857 ),
 .UNSPECIFIED., .F., .F.,
 ( 4, 4 ),
 ( 0.000000000000000000, 9.999999999998897304E-05 ),
 .UNSPECIFIED. ) ;
#78611=CARTESIAN_POINT ( 'NONE',  ( -3.453506354162970915, -21.03206338698385736, 11.49999999999999645 ) ) ;
#78614=CARTESIAN_POINT ( 'NONE',  ( 7.688942331755139747, 20.87172568467934752, 11.49999999999998934 ) ) ;
#78615=CARTESIAN_POINT ( 'NONE',  ( 10.45329875151443488, -17.81600612866554556, 11.49999999999998934 ) ) ;
#78616=ORIENTED_EDGE ( 'NONE', *, *, #9337, .T. ) ;
#78618=CARTESIAN_POINT ( 'NONE',  ( -95.54720254560318438, -24.63419186844610920, 9.035850630976922204 ) ) ;
#78620=CARTESIAN_POINT ( 'NONE',  ( -115.5228709571500616, -23.48786465467241769, 11.44779295918253759 ) ) ;
#78622=CARTESIAN_POINT ( 'NONE',  ( -49.58953762381672448, -23.48783264082478084, -1.443836473390070596 ) ) ;
#78623=CARTESIAN_POINT ( 'NONE',  ( -71.25210310630363608, -25.21189915732672659, 6.509906768301197744 ) ) ;
#78624=CARTESIAN_POINT ( 'NONE',  ( 4.135342931496230001, -20.44547621892628797, -1.500000000000002220 ) ) ;
#78625=EDGE_CURVE ( 'NONE', #16766, #86042, #78179, .T. ) ;
#78626=CARTESIAN_POINT ( 'NONE',  ( 0.003323472525107682655, -21.86402403546210493, 11.49999999999999645 ) ) ;
#78628=DIRECTION ( 'NONE',  ( 0.000000000000000000, 0.9999999999976377785, 2.173523156925979128E-06 ) ) ;
#78629=CARTESIAN_POINT ( 'NONE',  ( 20.52096793114426276, -9.243637136814692568, 11.49999999999998934 ) ) ;
#78630=CARTESIAN_POINT ( 'NONE',  ( -118.6249400182559413, -24.35071581493543746, 9.817618358456019934 ) ) ;
#78632=CARTESIAN_POINT ( 'NONE',  ( -59.62287095715007723, -23.47596703998600276, 11.44779298504227683 ) ) ;
#78633=ORIENTED_EDGE ( 'NONE', *, *, #24680, .T. ) ;
#78634=AXIS2_PLACEMENT_3D ( 'NONE', #87465, #46404, #77336 ) ;
#78635=EDGE_CURVE ( 'NONE', #58197, #73050, #96351, .T. ) ;
#78636=ORIENTED_EDGE ( 'NONE', *, *, #34577, .F. ) ;
#78637=ORIENTED_EDGE ( 'NONE', *, *, #61307, .F. ) ;
#78638=EDGE_CURVE ( 'NONE', #13348, #63463, #56289, .T. ) ;
#78640=CARTESIAN_POINT ( 'NONE',  ( 15.12546962493697933, 15.13007008128210096, -1.500000000000002220 ) ) ;
#78641=CARTESIAN_POINT ( 'NONE',  ( -9.622923231576368863, -20.19340101508991125, 11.49999999999999645 ) ) ;
#78642=ORIENTED_EDGE ( 'NONE', *, *, #88660, .T. ) ;
#78643=CARTESIAN_POINT ( 'NONE',  ( 19.40125262130244366, -8.172613994405130811, -1.500000000000002220 ) ) ;
#78644=CARTESIAN_POINT ( 'NONE',  ( -30.48447787840913392, -24.66679253312401698, 8.908675929220798650 ) ) ;
#78645=CARTESIAN_POINT ( 'NONE',  ( 2.927915493035635031, 19.71835975189664936, -1.500000000000002220 ) ) ;
#78646=CARTESIAN_POINT ( 'NONE',  ( -50.62611156557186121, -24.92592662359560762, 8.075495903017996469 ) ) ;
#78647=CARTESIAN_POINT ( 'NONE',  ( -61.62287095715004881, -23.48783264082478439, -1.443836473390069042 ) ) ;
#78648=CARTESIAN_POINT ( 'NONE',  ( -10.13730173486854369, -19.54584281717935568, -1.500000000000002220 ) ) ;
#78649=CARTESIAN_POINT ( 'NONE',  ( -83.52287095715009002, -24.33832256527049509, 0.1851278514138626485 ) ) ;
#78650=ORIENTED_EDGE ( 'NONE', *, *, #80131, .T. ) ;
#78651=CARTESIAN_POINT ( 'NONE',  ( -102.5228709571500758, -24.64898659630367916, 1.056161002820829697 ) ) ;
#78654=CARTESIAN_POINT ( 'NONE',  ( -16.21995886604411297, 13.06735728859114509, 11.49999999999999645 ) ) ;
#78658=CARTESIAN_POINT ( 'NONE',  ( -18.01091527469349529, -11.40912366963296698, -1.500000000000002220 ) ) ;
#78659=DIRECTION ( 'NONE',  ( -3.773278334453079030E-23, 0.9999999999976377785, 2.173523156925979128E-06 ) ) ;
#78660=B_SPLINE_CURVE_WITH_KNOTS ( 'NONE', 3,
 ( #62057, #53948, #7756, #46831, #15358, #23974, #45826, #61062, #39201, #77747, #15861, #99585, #16868, #63066 ),
 .UNSPECIFIED., .F., .F.,
 ( 4, 2, 2, 2, 2, 2, 4 ),
 ( 1.915770205925381696E-16, 0.0001882564892122831591, 0.0003765129784243747397, 0.0007530259568485313379, 0.001129538935272687882, 0.001317795424484765991, 0.001506051913696843884 ),
 .UNSPECIFIED. ) ;
#78661=CARTESIAN_POINT ( 'NONE',  ( -66.62287095715009855, -23.94994826722565762, -0.6494450866342729167 ) ) ;
#78662=CARTESIAN_POINT ( 'NONE',  ( -71.62287095715005592, -24.65952944569304606, 1.056160979905699016 ) ) ;
#78664=CARTESIAN_POINT ( 'NONE',  ( -21.23328875057882570, -7.520457577684837247, -1.500000000000002220 ) ) ;
#78665=VECTOR ( 'NONE', #67790, 1000.000000000000114 ) ;
#78667=ORIENTED_EDGE ( 'NONE', *, *, #53059, .T. ) ;
#78668=CARTESIAN_POINT ( 'NONE',  ( -78.94303308397306296, -25.26642230834568537, 5.977536689587218177 ) ) ;
#78670=CARTESIAN_POINT ( 'NONE',  ( 6.681059570357060551, -18.48443787736713873, 11.49999999999999645 ) ) ;
#78671=CARTESIAN_POINT ( 'NONE',  ( -93.62287095715005592, -23.48786465467241769, 11.44779295918254114 ) ) ;
#78675=AXIS2_PLACEMENT_3D ( 'NONE', #60785, #91701, #22185 ) ;
#78676=CARTESIAN_POINT ( 'NONE',  ( -111.5228709571500616, -23.47593901973090524, -1.443836447538996204 ) ) ;
#78677=CARTESIAN_POINT ( 'NONE',  ( -88.88918693012689687, -25.27880950044345454, 5.947789066509454159 ) ) ;
#78678=CARTESIAN_POINT ( 'NONE',  ( -124.5216656005884062, -23.73791477778912551, 11.05961554403169878 ) ) ;
#78680=DIRECTION ( 'NONE',  ( -3.773278334453079618E-23, 0.9999999999976377785, 2.173523156925979975E-06 ) ) ;
#78681=CARTESIAN_POINT ( 'NONE',  ( -3.970774856468506364, -19.35638658347046714, -1.500000000000002220 ) ) ;
#78682=ORIENTED_EDGE ( 'NONE', *, *, #34618, .T. ) ;
#78683=CARTESIAN_POINT ( 'NONE',  ( -14.42758394406654610, -14.16023863206117994, 11.49999999999999645 ) ) ;
#78687=ORIENTED_EDGE ( 'NONE', *, *, #29252, .F. ) ;
#78688=FACE_OUTER_BOUND ( 'NONE', #14207, .T. ) ;
#78689=CARTESIAN_POINT ( 'NONE',  ( -41.58953762381673158, -23.47596703998600276, 11.44779298504227505 ) ) ;
#78692=CARTESIAN_POINT ( 'NONE',  ( -41.58953762381673869, -24.66019654487199020, 8.947790411086133489 ) ) ;
#78694=CARTESIAN_POINT ( 'NONE',  ( 7.431233518514567926, -18.57414813805618081, 11.49999999999998934 ) ) ;
#78695=CARTESIAN_POINT ( 'NONE',  ( -79.52287095715006160, -29.50248528299804818, 1.056150453629038477 ) ) ;
#78696=CARTESIAN_POINT ( 'NONE',  ( -89.81226385320383088, -25.27367468601175204, 3.993462154588550916 ) ) ;
#78698=CARTESIAN_POINT ( 'NONE',  ( -79.51716134780556899, -23.73791477778911840, 11.05961554403170943 ) ) ;
#78699=B_SPLINE_CURVE_WITH_KNOTS ( 'NONE', 3,
 ( #70841, #17041, #48008, #71342, #77425, #16033 ),
 .UNSPECIFIED., .F., .F.,
 ( 4, 2, 4 ),
 ( 0.000000000000000000, 0.001380901958385382473, 0.002761803916770764946 ),
 .UNSPECIFIED. ) ;
#78700=CARTESIAN_POINT ( 'NONE',  ( -73.58953762381673869, -23.47596703998600276, 11.44779298504227683 ) ) ;
#78703=PLANE ( 'NONE',  #95051 ) ;
#78704=CARTESIAN_POINT ( 'NONE',  ( -83.50991238427990027, -24.15543982623907127, -0.2315651400026649820 ) ) ;
#78706=DIRECTION ( 'NONE',  ( 0.000000000000000000, -0.9999999999976377785, -2.173523156925979128E-06 ) ) ;
#78707=CARTESIAN_POINT ( 'NONE',  ( -84.55620429048340725, -24.64898659630528854, 1.056161002820828143 ) ) ;
#78708=EDGE_LOOP ( 'NONE', ( #15966, #81058, #17945, #82102 ) ) ;
#78710=CARTESIAN_POINT ( 'NONE',  ( 2.303441031721801480, -20.17751241584783628, -1.500000000000002220 ) ) ;
#78711=CARTESIAN_POINT ( 'NONE',  ( -115.2228709571500644, -23.47593901973090524, -1.443836447538996426 ) ) ;
#78712=PLANE ( 'NONE',  #40349 ) ;
#78714=CARTESIAN_POINT ( 'NONE',  ( -107.5228709571500758, -23.48786465467241769, 11.44779295918253936 ) ) ;
#78716=AXIS2_PLACEMENT_3D ( 'NONE', #31791, #70860, #84070 ) ;
#78717=ORIENTED_EDGE ( 'NONE', *, *, #53363, .F. ) ;
#78718=CARTESIAN_POINT ( 'NONE',  ( -86.52287095715003318, -23.73934037231757088, 11.05740245334329330 ) ) ;
#78719=CARTESIAN_POINT ( 'NONE',  ( -15.35229381799144299, -13.07563953244551591, -1.500000000000002220 ) ) ;
#78720=CARTESIAN_POINT ( 'NONE',  ( -12.37649675270136918, 17.12833386298736471, 11.49999999999999645 ) ) ;
#78721=EDGE_CURVE ( 'NONE', #37238, #29179, #87722, .T. ) ;
#78722=CARTESIAN_POINT ( 'NONE',  ( 21.58644828898399481, -4.983269013152989757, 11.49999999999998934 ) ) ;
#78723=CARTESIAN_POINT ( 'NONE',  ( -20.56140336115741718, 0.6910293267889283664, -1.500000000000002220 ) ) ;
#78725=CARTESIAN_POINT ( 'NONE',  ( -42.62287095715004881, -29.50250786944525672, 11.44777988621624232 ) ) ;
#78726=EDGE_LOOP ( 'NONE', ( #3381, #24579, #32831, #38709 ) ) ;
#78727=LINE ( 'NONE', #64060, #24951 ) ;
#78728=ORIENTED_EDGE ( 'NONE', *, *, #52057, .F. ) ;
#78729=DIRECTION ( 'NONE',  ( 0.000000000000000000, 2.173523156925980399E-06, -0.9999999999976378895 ) ) ;
#78730=FACE_OUTER_BOUND ( 'NONE', #19919, .T. ) ;
#78733=B_SPLINE_CURVE_WITH_KNOTS ( 'NONE', 3,
 ( #70868, #341, #15561, #85574 ),
 .UNSPECIFIED., .F., .F.,
 ( 4, 4 ),
 ( 0.07881234897532776729, 0.07981309601609325177 ),
 .UNSPECIFIED. ) ;
#78734=ORIENTED_EDGE ( 'NONE', *, *, #62971, .F. ) ;
#78736=ORIENTED_EDGE ( 'NONE', *, *, #50792, .T. ) ;
#78737=CARTESIAN_POINT ( 'NONE',  ( -81.62287095715005592, -24.50321055353803956, 9.387540953477527594 ) ) ;
#78738=CARTESIAN_POINT ( 'NONE',  ( -127.6228709571501412, -24.35013146730205236, 9.818937971375101270 ) ) ;
#78740=CARTESIAN_POINT ( 'NONE',  ( -14.56105648253378781, -14.73650127990469016, -1.500000000000002220 ) ) ;
#78741=EDGE_CURVE ( 'NONE', #93091, #76257, #75962, .T. ) ;
#78743=CARTESIAN_POINT ( 'NONE',  ( 12.10466045530642631, 18.00204671274030233, 11.49999999999999645 ) ) ;
#78744=ORIENTED_EDGE ( 'NONE', *, *, #74730, .F. ) ;
#78746=CARTESIAN_POINT ( 'NONE',  ( -102.6228709571500559, -29.50250786944525672, 11.44777988621623166 ) ) ;
#78747=CARTESIAN_POINT ( 'NONE',  ( 8.126467401150291536, 20.86698325809501497, -1.500000000000002220 ) ) ;
#78749=CARTESIAN_POINT ( 'NONE',  ( -66.92287095715005307, -23.47596703998600276, 11.44779298504227860 ) ) ;
#78751=EDGE_LOOP ( 'NONE', ( #7736, #87267, #62164, #29599 ) ) ;
#78753=CARTESIAN_POINT ( 'NONE',  ( -52.62287095715005592, -24.64965695001467694, 8.947790433994185832 ) ) ;
#78754=VERTEX_POINT ( 'NONE', #5467 ) ;
#78756=CARTESIAN_POINT ( 'NONE',  ( -87.62287095715001328, -23.48786465467241769, 11.44779295918254114 ) ) ;
#78760=CARTESIAN_POINT ( 'NONE',  ( -13.45780860896912934, -16.40347334334247265, -1.500000000000002220 ) ) ;
#78761=EDGE_CURVE ( 'NONE', #46787, #79347, #98808, .T. ) ;
#78763=DIRECTION ( 'NONE',  ( -3.773278334453079030E-23, 0.9999999999976377785, 2.173523156925979128E-06 ) ) ;
#78764=CARTESIAN_POINT ( 'NONE',  ( 8.287826148123016878, -20.17477452812186201, -1.500000000000002220 ) ) ;
#78765=CARTESIAN_POINT ( 'NONE',  ( -52.56778115561136389, -23.48786465467241058, 11.44779295918255357 ) ) ;
#78768=CARTESIAN_POINT ( 'NONE',  ( 21.06710269851327766, -5.618397932909799941, -1.500000000000002220 ) ) ;
#78771=CARTESIAN_POINT ( 'NONE',  ( -41.62287095715006302, -24.64898659630367561, 1.056161002820819261 ) ) ;
#78772=CARTESIAN_POINT ( 'NONE',  ( -48.91945971812886995, -25.12782585385058098, 6.515678671521449417 ) ) ;
#78773=EDGE_CURVE ( 'NONE', #44074, #70398, #21209, .T. ) ;
#78775=CARTESIAN_POINT ( 'NONE',  ( -129.6235879299834153, -24.35071581493544457, 9.817618358456021710 ) ) ;
#78777=EDGE_CURVE ( 'NONE', #2769, #81670, #3095, .T. ) ;
#78779=EDGE_CURVE ( 'NONE', #88839, #19118, #42987, .T. ) ;
#78783=CARTESIAN_POINT ( 'NONE',  ( -15.86343167427570577, 14.10970434637795634, 11.49999999999998934 ) ) ;
#78785=CARTESIAN_POINT ( 'NONE',  ( -30.59128290392954597, -24.93418366566757882, 8.369064737642425200 ) ) ;
#78786=CARTESIAN_POINT ( 'NONE',  ( -44.55620429048338593, -23.48786465467240347, 11.44779295918255180 ) ) ;
#78788=CARTESIAN_POINT ( 'NONE',  ( 15.46825748771582631, 11.69065726450791409, 11.49999999999998934 ) ) ;
#78789=CARTESIAN_POINT ( 'NONE',  ( -45.58893347773089744, -24.52300882791528380, 0.6510814631126234930 ) ) ;
#78790=ORIENTED_EDGE ( 'NONE', *, *, #79662, .F. ) ;
#78791=CARTESIAN_POINT ( 'NONE',  ( -4.042178566331402045, 19.10766070095605684, 11.49999999999999645 ) ) ;
#78796=CARTESIAN_POINT ( 'NONE',  ( -89.63470083817112766, -23.96119346886881019, -0.6495511937831908167 ) ) ;
#78798=CARTESIAN_POINT ( 'NONE',  ( -30.57287095715004099, -23.47593903913510260, -1.434903445928520149 ) ) ;
#78799=CARTESIAN_POINT ( 'NONE',  ( -101.0975906728528884, -25.21813695808114630, 3.546416755389510289 ) ) ;
#78800=CARTESIAN_POINT ( 'NONE',  ( -19.61143073682725202, -1.510137823221562092, -1.500000000000002220 ) ) ;
#78802=CARTESIAN_POINT ( 'NONE',  ( 20.55510029441247610, -6.647428040031946317, 11.49999999999998934 ) ) ;
#78804=CARTESIAN_POINT ( 'NONE',  ( 22.94779996701378266, 2.684060219229261968, -1.500000000000002220 ) ) ;
#78808=CARTESIAN_POINT ( 'NONE',  ( -115.5228709571500474, -23.47593901973090524, -1.443836447538996204 ) ) ;
#78809=CARTESIAN_POINT ( 'NONE',  ( -97.55239203327073483, -24.15620529776628800, 10.23563542870660115 ) ) ;
#78813=DIRECTION ( 'NONE',  ( 0.000000000000000000, 0.9999999999976377785, 2.173523156925979975E-06 ) ) ;
#78814=CARTESIAN_POINT ( 'NONE',  ( -129.5219952696967312, -24.15543982623907482, -0.2315651400026527140 ) ) ;
#78815=B_SPLINE_CURVE_WITH_KNOTS ( 'NONE', 3,
 ( #9379, #86505, #47957, #78878, #32716, #63700 ),
 .UNSPECIFIED., .F., .F.,
 ( 4, 2, 4 ),
 ( 0.000000000000000000, 0.001380764517854768218, 0.002761529035709536437 ),
 .UNSPECIFIED. ) ;
#78816=CARTESIAN_POINT ( 'NONE',  ( -114.5180505893580829, -24.15620529776629510, 10.23563542870659404 ) ) ;
#78817=CARTESIAN_POINT ( 'NONE',  ( -4.359361796094493258, -19.42695174060331809, -1.500000000000002220 ) ) ;
#78818=CARTESIAN_POINT ( 'NONE',  ( -75.48965661426149154, -25.00182538069146787, 7.747789668545045139 ) ) ;
#78819=CARTESIAN_POINT ( 'NONE',  ( 19.22361159462649027, -4.937694622890139939, -1.500000000000002220 ) ) ;
#78822=CARTESIAN_POINT ( 'NONE',  ( -56.64375047002581454, -23.96119346886880663, -0.6495511937832126881 ) ) ;
#78823=DIRECTION ( 'NONE',  ( -3.773278334453079618E-23, 0.9999999999976377785, 2.173523156925979975E-06 ) ) ;
#78825=CARTESIAN_POINT ( 'NONE',  ( 20.64725891757762355, 2.036748910689437864, 11.49999999999999645 ) ) ;
#78826=PLANE ( 'NONE',  #80733 ) ;
#78827=PLANE ( 'NONE',  #63600 ) ;
#78828=CARTESIAN_POINT ( 'NONE',  ( 21.64774270073068863, 7.000884456547583845, 11.49999999999999645 ) ) ;
#78829=ORIENTED_EDGE ( 'NONE', *, *, #55333, .T. ) ;
#78830=ADVANCED_FACE ( 'NONE', ( #8962 ), #31308, .T. ) ;
#78831=CARTESIAN_POINT ( 'NONE',  ( -83.62287095715007013, -23.48786465467241769, 11.44779295918254469 ) ) ;
#78832=CARTESIAN_POINT ( 'NONE',  ( -38.52287095715007581, -24.34917612407050314, 0.1852690917482237298 ) ) ;
#78833=EDGE_CURVE ( 'NONE', #61303, #63682, #25181, .T. ) ;
#78835=CARTESIAN_POINT ( 'NONE',  ( -17.27845874757997535, -10.49745931960568335, -1.500000000000002220 ) ) ;
#78839=EDGE_CURVE ( 'NONE', #92960, #87632, #70826, .T. ) ;
#78840=ADVANCED_FACE ( 'NONE', ( #93692 ), #1379, .T. ) ;
#78841=ORIENTED_EDGE ( 'NONE', *, *, #29755, .F. ) ;
#78842=CARTESIAN_POINT ( 'NONE',  ( -0.1426030150137709562, -21.20389190742572083, 11.50200000000000422 ) ) ;
#78843=CARTESIAN_POINT ( 'NONE',  ( 10.67403711042701353, -20.27515232684288549, 11.49999999999998934 ) ) ;
#78844=CARTESIAN_POINT ( 'NONE',  ( -30.50620355861343214, -23.47596700323886409, 11.43088626683780618 ) ) ;
#78845=CARTESIAN_POINT ( 'NONE',  ( -17.55682386033230102, 9.526633247210019917, -1.500000000000002220 ) ) ;
#78847=CARTESIAN_POINT ( 'NONE',  ( 5.724939850241691275, 20.19279902153374096, 11.49999999999999645 ) ) ;
#78848=EDGE_CURVE ( 'NONE', #52932, #21474, #18689, .T. ) ;
#78850=FACE_OUTER_BOUND ( 'NONE', #87038, .T. ) ;
#78852=CARTESIAN_POINT ( 'NONE',  ( 4.500060333422437608, -21.59917750860068963, -1.500000000000002220 ) ) ;
#78854=VERTEX_POINT ( 'NONE', #87596 ) ;
#78857=CARTESIAN_POINT ( 'NONE',  ( -40.01839366089613748, -25.29500187561385260, 5.509688069775453556 ) ) ;
#78859=CARTESIAN_POINT ( 'NONE',  ( -92.92287095715005307, -23.47596703998600631, 11.44779298504227860 ) ) ;
#78863=PLANE ( 'NONE',  #56801 ) ;
#78864=CARTESIAN_POINT ( 'NONE',  ( -100.5228709571500616, -23.47596703998600631, 11.44779298504228215 ) ) ;
#78865=CARTESIAN_POINT ( 'NONE',  ( -20.18818894172909140, 3.697778396234267184, -1.500000000000002220 ) ) ;
#78866=EDGE_CURVE ( 'NONE', #11910, #74791, #95703, .T. ) ;
#78868=CARTESIAN_POINT ( 'NONE',  ( -100.1362965613156319, -25.30290612096174030, 5.258114224706423201 ) ) ;
#78869=CARTESIAN_POINT ( 'NONE',  ( -44.64704124524567419, -23.96119346886879597, -0.6495511937832129101 ) ) ;
#78871=CARTESIAN_POINT ( 'NONE',  ( -22.23078454666273274, -1.437644496696519170, 11.49999999999998934 ) ) ;
#78873=CARTESIAN_POINT ( 'NONE',  ( -55.52287095715007581, -24.63345952396254290, 9.038047939301506517 ) ) ;
#78875=EDGE_CURVE ( 'NONE', #94218, #99569, #74421, .T. ) ;
#78878=CARTESIAN_POINT ( 'NONE',  ( -124.6228709571499706, -24.33832256527049154, 0.1851278514138684494 ) ) ;
#78879=CARTESIAN_POINT ( 'NONE',  ( 16.93201058511109380, 12.15574511561022852, 11.49999999999998934 ) ) ;
#78880=ORIENTED_EDGE ( 'NONE', *, *, #19402, .T. ) ;
#78882=EDGE_CURVE ( 'NONE', #12709, #77171, #72103, .T. ) ;
#78887=CARTESIAN_POINT ( 'NONE',  ( 20.99820426035194032, -0.1900765340283884497, -1.500000000000002220 ) ) ;
#78888=VERTEX_POINT ( 'NONE', #96696 ) ;
#78890=CARTESIAN_POINT ( 'NONE',  ( -118.5228709571500758, -24.33927499327856125, 9.819080762295802955 ) ) ;
#78891=DIRECTION ( 'NONE',  ( 0.000000000000000000, 0.9999999999976377785, 2.173523156925979128E-06 ) ) ;
#78894=CARTESIAN_POINT ( 'NONE',  ( -86.58836611889687163, -24.35071581493543391, 9.817618358456027039 ) ) ;
#78895=CARTESIAN_POINT ( 'NONE',  ( -59.64909978345416164, -23.73766607897669445, -1.055555164236460675 ) ) ;
#78896=CARTESIAN_POINT ( 'NONE',  ( -109.7567236225155511, -25.29789953159075466, 5.668539300329492825 ) ) ;
#78897=CARTESIAN_POINT ( 'NONE',  ( -63.58953762381673869, -24.64898659630528499, 1.056161002820821704 ) ) ;
#78898=CARTESIAN_POINT ( 'NONE',  ( -21.98633505697190671, -3.258044352128648846, 11.49999999999999645 ) ) ;
#78900=B_SPLINE_CURVE_WITH_KNOTS ( 'NONE', 3,
 ( #27001, #72682, #42741, #41231, #2675, #88404 ),
 .UNSPECIFIED., .F., .F.,
 ( 4, 2, 4 ),
 ( 1.570755371633816901E-05, 0.001396183895866086886, 0.002776660238015835579 ),
 .UNSPECIFIED. ) ;
#78901=LINE ( 'NONE', #17516, #38897 ) ;
#78902=CARTESIAN_POINT ( 'NONE',  ( -54.62287095715005592, -24.64898659630528854, 1.056161002820821038 ) ) ;
#78903=EDGE_LOOP ( 'NONE', ( #19289, #85929, #70594, #37856 ) ) ;
#78904=CARTESIAN_POINT ( 'NONE',  ( 14.05383982582471170, -17.77673030755399708, 11.49999999999998934 ) ) ;
#78905=B_SPLINE_CURVE_WITH_KNOTS ( 'NONE', 3,
 ( #21657, #52631, #68854, #1351 ),
 .UNSPECIFIED., .F., .F.,
 ( 4, 4 ),
 ( 0.6409576921988818787, 0.6499641234709975235 ),
 .UNSPECIFIED. ) ;
#78906=B_SPLINE_CURVE_WITH_KNOTS ( 'NONE', 3,
 ( #71800, #70294, #94621, #57085, #25102, #71295 ),
 .UNSPECIFIED., .F., .F.,
 ( 4, 2, 4 ),
 ( 6.384118695832212569E-06, 0.001386860460836989405, 0.002767336802978146663 ),
 .UNSPECIFIED. ) ;
#78907=B_SPLINE_CURVE_WITH_KNOTS ( 'NONE', 3,
 ( #83666, #67459, #6048, #45127 ),
 .UNSPECIFIED., .F., .F.,
 ( 4, 4 ),
 ( 0.7110077132042242898, 0.7200141444763397125 ),
 .UNSPECIFIED. ) ;
#78908=EDGE_CURVE ( 'NONE', #22695, #3935, #19946, .T. ) ;
#78911=EDGE_LOOP ( 'NONE', ( #67424, #94220, #72439, #1383 ) ) ;
#78913=ADVANCED_FACE ( 'NONE', ( #58153 ), #80977, .F. ) ;
#78914=CARTESIAN_POINT ( 'NONE',  ( 20.11291949428234105, -1.170665973999911902, -1.500000000000002220 ) ) ;
#78917=PLANE ( 'NONE',  #6595 ) ;
#78918=CARTESIAN_POINT ( 'NONE',  ( 21.53444271425275858, 6.169869319618734416, -1.500000000000002220 ) ) ;
#78920=ORIENTED_EDGE ( 'NONE', *, *, #66367, .T. ) ;
#78922=CARTESIAN_POINT ( 'NONE',  ( -94.54933745284346003, -24.35071581493543036, 9.817618358456030592 ) ) ;
#78925=CARTESIAN_POINT ( 'NONE',  ( -124.5228709571500190, -24.66019654487200441, 8.947790411086112172 ) ) ;
#78927=CARTESIAN_POINT ( 'NONE',  ( -15.85469643196389278, -11.46343829903102396, 11.49999999999998934 ) ) ;
#78928=DIRECTION ( 'NONE',  ( 3.773278334444167608E-23, -1.000000000000000000, 0.000000000000000000 ) ) ;
#78929=EDGE_LOOP ( 'NONE', ( #86712, #93603, #93610, #57326 ) ) ;
#78930=CARTESIAN_POINT ( 'NONE',  ( -5.607854029519995898, -20.77141283803394955, -1.500000000000002220 ) ) ;
#78931=AXIS2_PLACEMENT_3D ( 'NONE', #80683, #58361, #26401 ) ;
#78932=CARTESIAN_POINT ( 'NONE',  ( -62.52287095715003318, -24.66019654487199730, 8.947790411086124607 ) ) ;
#78934=CARTESIAN_POINT ( 'NONE',  ( -100.7575127936760566, -25.12643199199673560, 2.865359487688054152 ) ) ;
#78935=CARTESIAN_POINT ( 'NONE',  ( -107.5562042904834072, -23.47596703998600631, 11.44779298504227683 ) ) ;
#78936=CARTESIAN_POINT ( 'NONE',  ( -3.987988226355533072, 22.59150145119509290, -1.500000000000002220 ) ) ;
#78937=B_SPLINE_CURVE_WITH_KNOTS ( 'NONE', 3,
 ( #84518, #38344, #69298, #100216 ),
 .UNSPECIFIED., .F., .F.,
 ( 4, 4 ),
 ( 6.656022119059916131E-09, 0.002563024260995911199 ),
 .UNSPECIFIED. ) ;
#78941=CARTESIAN_POINT ( 'NONE',  ( -1.723993941171178879, -19.98520929721398431, 11.49999999999999645 ) ) ;
#78942=CARTESIAN_POINT ( 'NONE',  ( -79.79643364552497076, -25.26612395677430456, 4.606720527762783846 ) ) ;
#78944=B_SPLINE_CURVE_WITH_KNOTS ( 'NONE', 3,
 ( #25543, #56010, #26551, #56511 ),
 .UNSPECIFIED., .F., .F.,
 ( 4, 4 ),
 ( 0.000000000000000000, 9.999999999998898659E-05 ),
 .UNSPECIFIED. ) ;
#78946=DIRECTION ( 'NONE',  ( -3.773278334453079618E-23, 0.9999999999976377785, 2.173523156925978705E-06 ) ) ;
#78947=CARTESIAN_POINT ( 'NONE',  ( -85.62287095715011276, -24.51163499207176244, 0.6490370598554221493 ) ) ;
#78948=CARTESIAN_POINT ( 'NONE',  ( 6.829227106855087825, -20.66181959361685827, -1.500000000000002220 ) ) ;
#78950=CARTESIAN_POINT ( 'NONE',  ( 18.19143915067776263, 7.407926943018095400, -1.500000000000002220 ) ) ;
#78951=VECTOR ( 'NONE', #87284, 1000.000000000000114 ) ;
#78952=CARTESIAN_POINT ( 'NONE',  ( -61.59189125704997281, -25.08279362854488781, 7.371166896404004909 ) ) ;
#78953=CARTESIAN_POINT ( 'NONE',  ( -109.3951644950792996, -25.31698007842469877, 4.495754895749054292 ) ) ;
#78955=CARTESIAN_POINT ( 'NONE',  ( -91.51495999646013502, -23.96169478059713498, 10.65365249895718058 ) ) ;
#78957=CARTESIAN_POINT ( 'NONE',  ( 15.43701773751798001, -13.56989305476470875, 11.49999999999999645 ) ) ;
#78959=VECTOR ( 'NONE', #29336, 1000.000000000000114 ) ;
#78961=CARTESIAN_POINT ( 'NONE',  ( -3.174168706971715270, 22.36591850054903929, 11.49999999999999645 ) ) ;
#78962=ORIENTED_EDGE ( 'NONE', *, *, #43698, .F. ) ;
#78963=CARTESIAN_POINT ( 'NONE',  ( -46.62287095715004170, -24.51283580621364067, 0.6167428607019801445 ) ) ;
#78964=CARTESIAN_POINT ( 'NONE',  ( -60.52287095715006160, -24.99132157543083821, 2.256160258750667502 ) ) ;
#78965=CARTESIAN_POINT ( 'NONE',  ( -125.5887522299914139, -25.00182538069147498, 7.747789668545045139 ) ) ;
#78967=CARTESIAN_POINT ( 'NONE',  ( -62.62287095715004881, -23.48783264082478794, -1.443836473390068820 ) ) ;
#78971=EDGE_CURVE ( 'NONE', #89924, #85031, #5408, .T. ) ;
#78975=CARTESIAN_POINT ( 'NONE',  ( -79.64180909446726275, -25.31596281824522165, 5.241605647354496966 ) ) ;
#78976=CARTESIAN_POINT ( 'NONE',  ( 22.79674358141071977, 1.614764915196592598, 11.49999999999998934 ) ) ;
#78978=CARTESIAN_POINT ( 'NONE',  ( -96.54562372648371138, -24.65952944569305316, 1.056160979905706121 ) ) ;
#78979=CARTESIAN_POINT ( 'NONE',  ( -63.59779687502174994, -23.96169478059713143, 10.65365249895718236 ) ) ;
#78980=CARTESIAN_POINT ( 'NONE',  ( 16.82713599508461400, -14.87465808564757808, 11.49999999999999645 ) ) ;
#78982=CARTESIAN_POINT ( 'NONE',  ( -70.62287095715002749, -24.83620972994591369, 8.398175272781363887 ) ) ;
#78983=CARTESIAN_POINT ( 'NONE',  ( 6.821863743248424150, 20.85434273413645911, 11.49999999999998934 ) ) ;
#78984=CARTESIAN_POINT ( 'NONE',  ( -125.0508430453642319, -25.34741532608440906, 3.801652799235191615 ) ) ;
#78985=CARTESIAN_POINT ( 'NONE',  ( -34.60965091549643802, -23.73791477778911485, 11.05961554403171299 ) ) ;
#78986=CARTESIAN_POINT ( 'NONE',  ( -121.5228709571500616, -23.47596703998600631, 11.44779298504227860 ) ) ;
#78987=ORIENTED_EDGE ( 'NONE', *, *, #16772, .F. ) ;
#78988=ADVANCED_FACE ( 'NONE', ( #40242 ), #25001, .T. ) ;
#78992=CARTESIAN_POINT ( 'NONE',  ( -15.03541999946025243, -13.88573836563254460, 11.49999999999998934 ) ) ;
#78998=CARTESIAN_POINT ( 'NONE',  ( 15.98122378838116120, 16.67787885001082770, 11.49999999999998934 ) ) ;
#78999=CARTESIAN_POINT ( 'NONE',  ( -39.43364804524359357, -25.30977039686255026, 4.487062071701387822 ) ) ;
#79000=CARTESIAN_POINT ( 'NONE',  ( -19.38859340154505873, -6.080128201517944753, -1.500000000000002220 ) ) ;
#79001=ORIENTED_EDGE ( 'NONE', *, *, #54479, .F. ) ;
#79003=CARTESIAN_POINT ( 'NONE',  ( -101.7776484685884100, -25.27307239909451653, 3.986250617436227550 ) ) ;
#79004=DIRECTION ( 'NONE',  ( -3.773278334453079618E-23, 0.9999999999976377785, 2.173523156925979975E-06 ) ) ;
#79005=CARTESIAN_POINT ( 'NONE',  ( -93.62287095715005592, -24.64965695001468404, 8.947790433994180503 ) ) ;
#79007=CARTESIAN_POINT ( 'NONE',  ( 7.367719877546908158, -20.20905560389912026, 11.49999999999999645 ) ) ;
#79008=VERTEX_POINT ( 'NONE', #40738 ) ;
#79009=CARTESIAN_POINT ( 'NONE',  ( -75.54717685357564960, -24.40034930558991277, 0.3402023900116102895 ) ) ;
#79010=CARTESIAN_POINT ( 'NONE',  ( -112.5562042904834072, -24.64898659630529210, 1.056161002820830142 ) ) ;
#79012=VECTOR ( 'NONE', #17809, 1000.000000000000114 ) ;
#79013=CARTESIAN_POINT ( 'NONE',  ( -5.954758479537505700, 19.85987847461844424, 11.49999999999998934 ) ) ;
#79014=VERTEX_POINT ( 'NONE', #54467 ) ;
#79015=CARTESIAN_POINT ( 'NONE',  ( -125.5540159630755284, -25.00158670708911046, 2.256160236439218369 ) ) ;
#79017=B_SPLINE_SURFACE_WITH_KNOTS ( 'NONE', 3, 3, ( 
 ( #28730, #97735, #65328, #66314 ),
 ( #43464, #74886, #97241, #11999 ),
 ( #82505, #57694, #72917, #19607 ),
 ( #34847, #74401, #65816, #81020 ),
 ( #50081, #3415, #11008, #96248 ),
 ( #42968, #11499, #51572, #27732 ),
 ( #19109, #26732, #88639, #81525 ),
 ( #43952, #96740, #5389, #42478 ),
 ( #12499, #90127, #34350, #20605 ),
 ( #35841, #4895, #18608, #58192 ) ),
 .UNSPECIFIED., .F., .F., .F.,
 ( 4, 3, 3, 4 ),
 ( 4, 4 ),
 ( 0.0004766839783816634356, 0.1491231665100169745, 0.2234464077758346323, 0.2977696490416522623 ),
 ( 0.2495241339546893922, 0.2506855492118910123 ),
 .UNSPECIFIED. ) ;
#79018=CARTESIAN_POINT ( 'NONE',  ( -75.62287095715004170, -24.91570333823099759, 8.075032458375554612 ) ) ;
#79019=PLANE ( 'NONE',  #29197 ) ;
#79021=ORIENTED_EDGE ( 'NONE', *, *, #75310, .F. ) ;
#79023=CARTESIAN_POINT ( 'NONE',  ( -42.57642875886570977, -24.66019654487198665, 8.947790411086131712 ) ) ;
#79024=CARTESIAN_POINT ( 'NONE',  ( -27.89246614958421944, -24.63140169414405278, 1.634486445453936954 ) ) ;
#79025=CARTESIAN_POINT ( 'NONE',  ( -12.30081598482267680, 18.28176383447183895, 11.49999999999999645 ) ) ;
#79027=CARTESIAN_POINT ( 'NONE',  ( -103.6358262473195708, -23.48783264082477018, -1.443836473390091246 ) ) ;
#79028=CARTESIAN_POINT ( 'NONE',  ( 7.090404290683943067, 21.45231405096426514, 11.49999999999998934 ) ) ;
#79031=CARTESIAN_POINT ( 'NONE',  ( 12.86141378215833342, 16.59024694808438127, 11.49999999999998934 ) ) ;
#79032=CARTESIAN_POINT ( 'NONE',  ( -70.62287095715011276, -24.82558206586143257, 1.605769216559449708 ) ) ;
#79033=ORIENTED_EDGE ( 'NONE', *, *, #85996, .T. ) ;
#79036=ADVANCED_FACE ( 'NONE', ( #87409 ), #1181, .T. ) ;
#79037=VECTOR ( 'NONE', #50949, 1000.000000000000114 ) ;
#79038=EDGE_CURVE ( 'NONE', #58867, #32620, #51411, .T. ) ;
#79041=CARTESIAN_POINT ( 'NONE',  ( 12.34367313097222763, -17.18290682204727915, -1.500000000000002220 ) ) ;
#79043=CARTESIAN_POINT ( 'NONE',  ( -61.66078443741151460, -25.31249728293746770, 5.276660823416809087 ) ) ;
#79044=CARTESIAN_POINT ( 'NONE',  ( -104.6228709571500559, -24.64965695001468404, 8.947790433994178727 ) ) ;
#79046=CARTESIAN_POINT ( 'NONE',  ( -125.6228709571499706, -24.91544648472619983, 1.928969306349219259 ) ) ;
#79048=CARTESIAN_POINT ( 'NONE',  ( 22.02009960291501045, 3.200778107580485532, -1.500000000000002220 ) ) ;
#79049=B_SPLINE_CURVE_WITH_KNOTS ( 'NONE', 3,
 ( #73732, #35181, #94191, #86086, #93190, #25182, #62777, #32805, #55660, #86586, #77954, #23676, #24183, #2365 ),
 .UNSPECIFIED., .F., .F.,
 ( 4, 2, 2, 2, 2, 2, 4 ),
 ( 0.000000000000000000, 0.0002304994410172846522, 0.0004609988820345693045, 0.0009219977640691386089, 0.001382996646103707913, 0.001613496087120987795, 0.001843995528138267460 ),
 .UNSPECIFIED. ) ;
#79050=CARTESIAN_POINT ( 'NONE',  ( -114.5904446279929232, -24.15543982623908192, -0.2315651400026444429 ) ) ;
#79051=VERTEX_POINT ( 'NONE', #85402 ) ;
#79053=CARTESIAN_POINT ( 'NONE',  ( -37.53883053087279364, -24.34968618360933590, 0.1864209137778856384 ) ) ;
#79055=CARTESIAN_POINT ( 'NONE',  ( -41.72911611951712985, -25.22311787329266153, 3.586264385156655354 ) ) ;
#79057=CARTESIAN_POINT ( 'NONE',  ( 6.171429453590791425, 18.48145409631445446, 11.49999999999998934 ) ) ;
#79058=CARTESIAN_POINT ( 'NONE',  ( 19.34736296927903254, -9.154118057783460216, -1.500000000000002220 ) ) ;
#79059=CARTESIAN_POINT ( 'NONE',  ( -85.52287095715009002, -23.84081130425357742, 10.88220057483159842 ) ) ;
#79060=CARTESIAN_POINT ( 'NONE',  ( -60.57606894313024526, -25.00182538069856619, 7.747789668514392325 ) ) ;
#79061=CARTESIAN_POINT ( 'NONE',  ( -78.52287095715004739, -23.48783264082476308, -1.443836473390091468 ) ) ;
#79062=CARTESIAN_POINT ( 'NONE',  ( -100.7282901814618583, -25.18440018975361028, 3.329830012351928215 ) ) ;
#79063=B_SPLINE_CURVE_WITH_KNOTS ( 'NONE', 3,
 ( #31501, #9166, #18287, #54857, #1572, #10676 ),
 .UNSPECIFIED., .F., .F.,
 ( 4, 2, 4 ),
 ( 1.570887131794333942E-05, 0.001396322306279758904, 0.002776935741241574537 ),
 .UNSPECIFIED. ) ;
#79064=CARTESIAN_POINT ( 'NONE',  ( -22.19569011343799048, 5.130922947863589378, -1.500000000000002220 ) ) ;
#79065=CARTESIAN_POINT ( 'NONE',  ( -103.6228709571500701, -23.48783264082478794, -1.443836473390062158 ) ) ;
#79066=CARTESIAN_POINT ( 'NONE',  ( -80.52287095715007581, -24.51163499207174823, 0.6490370598554294768 ) ) ;
#79067=CARTESIAN_POINT ( 'NONE',  ( 4.164567180745167185, 19.39263604865329071, 11.49999999999999645 ) ) ;
#79068=CARTESIAN_POINT ( 'NONE',  ( -123.5895113708369593, -24.35071581493544812, 9.817618358456018157 ) ) ;
#79071=VERTEX_POINT ( 'NONE', #56488 ) ;
#79074=CARTESIAN_POINT ( 'NONE',  ( -51.04701396381788925, -25.10935790734607664, 2.986906079344115561 ) ) ;
#79075=CARTESIAN_POINT ( 'NONE',  ( -21.36891742734480104, 3.643610035731704055, -1.500000000000002220 ) ) ;
#79076=DIRECTION ( 'NONE',  ( 0.000000000000000000, 0.9999999999976377785, 2.173523156925979128E-06 ) ) ;
#79077=CARTESIAN_POINT ( 'NONE',  ( -8.858824863812619910, -17.32749669425128047, -1.500000000000002220 ) ) ;
#79079=EDGE_CURVE ( 'NONE', #19180, #99338, #6658, .T. ) ;
#79080=ORIENTED_EDGE ( 'NONE', *, *, #90013, .F. ) ;
#79081=CARTESIAN_POINT ( 'NONE',  ( -7.038884989605349141, -19.10714869031923513, 11.49999999999999645 ) ) ;
#79082=CARTESIAN_POINT ( 'NONE',  ( -99.12380231474227799, -25.27434709648489886, 4.001575133896465353 ) ) ;
#79084=ORIENTED_EDGE ( 'NONE', *, *, #53363, .T. ) ;
#79085=CARTESIAN_POINT ( 'NONE',  ( -78.94547585321313932, -25.25799298595097042, 6.082296582953498287 ) ) ;
#79087=CARTESIAN_POINT ( 'NONE',  ( -39.14714599385568761, -25.27985388593766203, 4.777938703530348441 ) ) ;
#79088=ADVANCED_FACE ( 'NONE', ( #32622 ), #17401, .F. ) ;
#79089=DIRECTION ( 'NONE',  ( -3.773278334453080206E-23, 0.9999999999976377785, 2.173523156925979975E-06 ) ) ;
#79091=CARTESIAN_POINT ( 'NONE',  ( 19.93115673323400117, -2.579441489355707606, 11.49999999999998934 ) ) ;
#79093=EDGE_CURVE ( 'NONE', #16766, #43974, #71697, .T. ) ;
#79096=VECTOR ( 'NONE', #54007, 1000.000000000000114 ) ;
#79097=EDGE_CURVE ( 'NONE', #35546, #40078, #33124, .T. ) ;
#79098=CARTESIAN_POINT ( 'NONE',  ( -22.87025945403008365, 2.249016246415321163, 11.49999999999999645 ) ) ;
#79099=CARTESIAN_POINT ( 'NONE',  ( 19.62911079104473444, -11.51699945595908758, -1.500000000000002220 ) ) ;
#79100=VERTEX_POINT ( 'NONE', #19392 ) ;
#79101=CARTESIAN_POINT ( 'NONE',  ( -30.47287095715007155, -24.04948693798736059, 10.44728643021711179 ) ) ;
#79104=CARTESIAN_POINT ( 'NONE',  ( -90.58935238007963164, -24.52300882791528380, 0.6510814631126311536 ) ) ;
#79105=B_SPLINE_CURVE_WITH_KNOTS ( 'NONE', 3,
 ( #52479, #91030, #82417, #66229, #89046, #51481 ),
 .UNSPECIFIED., .F., .F.,
 ( 4, 2, 4 ),
 ( 0.000000000000000000, 0.001380901958385378570, 0.002761803916770757140 ),
 .UNSPECIFIED. ) ;
#79107=CARTESIAN_POINT ( 'NONE',  ( -30.57287095715007652, -24.39156613236284343, 9.691265933976838554 ) ) ;
#79108=AXIS2_PLACEMENT_3D ( 'NONE', #25360, #47713, #78628 ) ;
#79109=CARTESIAN_POINT ( 'NONE',  ( -69.55395755889061604, -23.96169478059712787, 10.65365249895718414 ) ) ;
#79110=DIRECTION ( 'NONE',  ( 0.000000000000000000, -0.9999999999976377785, -2.173523156925979975E-06 ) ) ;
#79111=CARTESIAN_POINT ( 'NONE',  ( -122.5540053569840921, -24.51314013834316086, 0.6176544820404212821 ) ) ;
#79112=DIRECTION ( 'NONE',  ( -3.773278334453080206E-23, 0.9999999999976377785, 2.173523156925979975E-06 ) ) ;
#79115=CARTESIAN_POINT ( 'NONE',  ( -17.41452279269062586, 10.58001483151439004, 11.49999999999998934 ) ) ;
#79117=VERTEX_POINT ( 'NONE', #42755 ) ;
#79118=EDGE_CURVE ( 'NONE', #76771, #20796, #69570, .T. ) ;
#79119=CARTESIAN_POINT ( 'NONE',  ( 5.527175565732886042, -22.34193536506064603, 11.49999999999998934 ) ) ;
#79121=ORIENTED_EDGE ( 'NONE', *, *, #61127, .F. ) ;
#79123=CARTESIAN_POINT ( 'NONE',  ( -118.6228709571500701, -24.65952944569305316, 1.056160979905706565 ) ) ;
#79124=CARTESIAN_POINT ( 'NONE',  ( -95.56281893974220054, -23.48783264082477729, -1.443836473390088804 ) ) ;
#79126=VECTOR ( 'NONE', #7830, 1000.000000000000114 ) ;
#79127=CARTESIAN_POINT ( 'NONE',  ( -17.77299844720193533, 11.79293508692305537, 11.49999999999999645 ) ) ;
#79130=CARTESIAN_POINT ( 'NONE',  ( -17.21897301287555848, -14.04741862099043104, -1.500000000000002220 ) ) ;
#79131=CARTESIAN_POINT ( 'NONE',  ( -14.43086120294938368, -14.79396848081076854, 11.49999999999998934 ) ) ;
#79134=B_SPLINE_CURVE_WITH_KNOTS ( 'NONE', 3,
 ( #5258, #36216, #67676, #67180, #98596, #5756 ),
 .UNSPECIFIED., .F., .F.,
 ( 4, 2, 4 ),
 ( 1.570755371634415583E-05, 0.001396183895866091439, 0.002776660238015839048 ),
 .UNSPECIFIED. ) ;
#79135=CARTESIAN_POINT ( 'NONE',  ( -95.55370924776086383, -24.15602025860896163, 10.28564288303535967 ) ) ;
#79137=CARTESIAN_POINT ( 'NONE',  ( -28.62287095715004526, -24.50732993938405357, 8.947790418389013567 ) ) ;
#79139=CARTESIAN_POINT ( 'NONE',  ( -91.52287095715006160, -29.50250786944525672, 11.44777988621623344 ) ) ;
#79140=CARTESIAN_POINT ( 'NONE',  ( 16.07097863352054290, 13.35096362007907622, -1.500000000000002220 ) ) ;
#79141=CARTESIAN_POINT ( 'NONE',  ( 9.711643268838683341, -19.58466107313252635, 11.49999999999999645 ) ) ;
#79142=EDGE_CURVE ( 'NONE', #50701, #51171, #34635, .T. ) ;
#79143=B_SPLINE_CURVE_WITH_KNOTS ( 'NONE', 3,
 ( #1335, #93156, #55629, #71345, #16035, #62746 ),
 .UNSPECIFIED., .F., .F.,
 ( 4, 2, 4 ),
 ( 1.570755371634190273E-05, 0.001396183895866087536, 0.002776660238015833410 ),
 .UNSPECIFIED. ) ;
#79144=CARTESIAN_POINT ( 'NONE',  ( -27.47736343186643637, -24.89280002061735431, 7.597050255658339246 ) ) ;
#79146=CARTESIAN_POINT ( 'NONE',  ( 5.133194422563156500, 21.89913303424002677, 11.49999999999998934 ) ) ;
#79147=PLANE ( 'NONE',  #74098 ) ;
#79150=CARTESIAN_POINT ( 'NONE',  ( -59.55620429048340014, -23.47596703998600276, 11.44779298504227505 ) ) ;
#79151=VERTEX_POINT ( 'NONE', #27522 ) ;
#79154=CARTESIAN_POINT ( 'NONE',  ( -73.62287095715005592, -29.50250786944525672, 11.44777988621623699 ) ) ;
#79156=CARTESIAN_POINT ( 'NONE',  ( 19.34736296927903254, -9.154118057783460216, -1.500000000000002220 ) ) ;
#79157=CARTESIAN_POINT ( 'NONE',  ( -13.97600220251353953, -17.46790257487896270, 11.49999999999999645 ) ) ;
#79161=CARTESIAN_POINT ( 'NONE',  ( 20.56459456670464547, 4.482388377596099538, 11.49999999999998934 ) ) ;
#79162=CARTESIAN_POINT ( 'NONE',  ( -30.49547139261239082, -24.38102096386331752, 9.702671485061733492 ) ) ;
#79163=CARTESIAN_POINT ( 'NONE',  ( 4.608267332293128682, -19.41724391825443874, -1.500000000000002220 ) ) ;
#79164=CARTESIAN_POINT ( 'NONE',  ( -117.6228709571500701, -23.73907113216991860, -1.053371485793220153 ) ) ;
#79165=CARTESIAN_POINT ( 'NONE',  ( -61.55620429048339304, -23.48783264082478084, -1.443836473390068376 ) ) ;
#79166=CARTESIAN_POINT ( 'NONE',  ( -22.07534667767119174, -0.2742745133902674826, -1.500000000000002220 ) ) ;
#79167=ORIENTED_EDGE ( 'NONE', *, *, #95316, .T. ) ;
#79168=CARTESIAN_POINT ( 'NONE',  ( -116.5208660521144424, -23.73766607897671577, -1.055555164236427812 ) ) ;
#79170=CARTESIAN_POINT ( 'NONE',  ( -32.52287095715006160, -29.50250243563736774, 8.947779886222150481 ) ) ;
#79171=CARTESIAN_POINT ( 'NONE',  ( -17.86878485216894319, -10.78119150571587781, 11.49999999999999645 ) ) ;
#79175=CARTESIAN_POINT ( 'NONE',  ( -82.52287095715001897, -23.48783264083388289, -1.443836473375923690 ) ) ;
#79176=B_SPLINE_CURVE_WITH_KNOTS ( 'NONE', 3,
 ( #100188, #6378, #77366, #53066 ),
 .UNSPECIFIED., .F., .F.,
 ( 4, 4 ),
 ( 0.000000000000000000, 9.999999999998900014E-05 ),
 .UNSPECIFIED. ) ;
#79177=CARTESIAN_POINT ( 'NONE',  ( -21.15786647118399699, 2.672229404501205163, -1.500000000000002220 ) ) ;
#79178=CARTESIAN_POINT ( 'NONE',  ( -81.52287095715007581, -24.33832256527047733, 0.1851278514138612330 ) ) ;
#79179=DIRECTION ( 'NONE',  ( -3.773278334453079618E-23, 0.9999999999976377785, 2.173523156925979975E-06 ) ) ;
#79180=CARTESIAN_POINT ( 'NONE',  ( -111.9545732713065291, -25.06732945298220372, 7.447791367849804445 ) ) ;
#79181=FACE_OUTER_BOUND ( 'NONE', #57006, .T. ) ;
#79183=CARTESIAN_POINT ( 'NONE',  ( -20.69567741759225399, -9.018594580484563750, -1.500000000000002220 ) ) ;
#79184=CARTESIAN_POINT ( 'NONE',  ( -51.52287095715005449, -24.66019654487199375, 8.947790411086119278 ) ) ;
#79186=B_SPLINE_CURVE_WITH_KNOTS ( 'NONE', 3,
 ( #14140, #7039, #37991, #92269, #46111, #88545, #3818, #54730, #38986, #69936, #70951, #55735, #23250, #1440 ),
 .UNSPECIFIED., .F., .F.,
 ( 4, 2, 2, 2, 2, 2, 4 ),
 ( 0.000000000000000000, 0.0001585405595148470887, 0.0003170811190296941775, 0.0006341622380593686225, 0.0009512433570890431759, 0.001109783916603885061, 0.001268324476118726837 ),
 .UNSPECIFIED. ) ;
#79187=CARTESIAN_POINT ( 'NONE',  ( -78.94508464886243360, -25.27411879719900867, 5.881884475350567243 ) ) ;
#79188=CARTESIAN_POINT ( 'NONE',  ( -31.59415779167720117, -24.15620529776627379, 10.23563542870661536 ) ) ;
#79189=CARTESIAN_POINT ( 'NONE',  ( 0.7808950796103379943, -19.64173473864696717, 11.49999999999999645 ) ) ;
#79191=AXIS2_PLACEMENT_3D ( 'NONE', #69245, #39786, #15945 ) ;
#79193=EDGE_LOOP ( 'NONE', ( #62712, #81279, #84613, #1395 ) ) ;
#79194=CARTESIAN_POINT ( 'NONE',  ( -99.51646351673205970, -23.96119346886881374, -0.6495511937831867089 ) ) ;
#79195=DIRECTION ( 'NONE',  ( -3.773278334453079030E-23, 0.9999999999976377785, 2.173523156925979128E-06 ) ) ;
#79196=CARTESIAN_POINT ( 'NONE',  ( -105.5228709571500474, -23.85229601348996198, 10.88205029486208097 ) ) ;
#79198=CARTESIAN_POINT ( 'NONE',  ( 19.74453702311487646, -0.1846442961375113490, 11.49999999999998934 ) ) ;
#79199=B_SPLINE_CURVE_WITH_KNOTS ( 'NONE', 3,
 ( #87027, #63210, #94133, #17517 ),
 .UNSPECIFIED., .F., .F.,
 ( 4, 4 ),
 ( 0.000000000000000000, 9.999999999998897304E-05 ),
 .UNSPECIFIED. ) ;
#79201=CARTESIAN_POINT ( 'NONE',  ( -10.81679630089563915, -17.07601267366916886, 11.49999999999999645 ) ) ;
#79203=AXIS2_PLACEMENT_3D ( 'NONE', #63248, #54134, #31275 ) ;
#79204=ORIENTED_EDGE ( 'NONE', *, *, #87572, .F. ) ;
#79205=CARTESIAN_POINT ( 'NONE',  ( -67.52287095715003318, -23.73934037231757088, 11.05740245334328797 ) ) ;
#79207=CARTESIAN_POINT ( 'NONE',  ( -51.51908035862399515, -25.26093919477311900, 6.045684827221686319 ) ) ;
#79208=CARTESIAN_POINT ( 'NONE',  ( -125.5228709571500616, -29.50250243563736774, 8.947779886222132717 ) ) ;
#79210=CARTESIAN_POINT ( 'NONE',  ( -96.52287095715009002, -23.73907113216990084, -1.053371485793247686 ) ) ;
#79211=CARTESIAN_POINT ( 'NONE',  ( 5.980626343040887249, -19.09133569553460319, -1.500000000000002220 ) ) ;
#79212=EDGE_CURVE ( 'NONE', #51268, #803, #23526, .T. ) ;
#79213=CARTESIAN_POINT ( 'NONE',  ( -99.38436720317001516, -25.10935138625626450, 3.296897716455177818 ) ) ;
#79214=CARTESIAN_POINT ( 'NONE',  ( -116.5914120462304737, -23.96169478059714208, 10.65365249895717348 ) ) ;
#79220=EDGE_CURVE ( 'NONE', #55689, #13751, #88421, .T. ) ;
#79222=CARTESIAN_POINT ( 'NONE',  ( -83.63279703061509451, -24.15543982623906771, -0.2315651400026649265 ) ) ;
#79224=CARTESIAN_POINT ( 'NONE',  ( -49.72423105612087113, -25.21524731596653623, 3.522669676481375411 ) ) ;
#79225=EDGE_LOOP ( 'NONE', ( #47202, #41933, #80038, #8408 ) ) ;
#79228=CARTESIAN_POINT ( 'NONE',  ( 0.7445296356392017145, -20.29553345556499622, -1.500000000000002220 ) ) ;
#79229=EDGE_CURVE ( 'NONE', #78754, #53473, #18401, .T. ) ;
#79231=CARTESIAN_POINT ( 'NONE',  ( -34.62373370718334797, -24.65952944569304606, 1.056160979905694353 ) ) ;
#79233=CARTESIAN_POINT ( 'NONE',  ( -107.5228709571500900, -23.73934037231758154, 11.05740245334328442 ) ) ;
#79236=CARTESIAN_POINT ( 'NONE',  ( -10.65520286329281596, -18.28862552182625123, 11.49999999999999645 ) ) ;
#79237=AXIS2_PLACEMENT_3D ( 'NONE', #23027, #14432, #100144 ) ;
#79238=CARTESIAN_POINT ( 'NONE',  ( 0.7503028313155074569, 22.12739137992853955, -1.500000000000002220 ) ) ;
#79239=CARTESIAN_POINT ( 'NONE',  ( 13.18781518674367348, -15.76626393773247337, -1.500000000000002220 ) ) ;
#79240=ORIENTED_EDGE ( 'NONE', *, *, #32737, .F. ) ;
#79242=ORIENTED_EDGE ( 'NONE', *, *, #10773, .T. ) ;
#79243=CARTESIAN_POINT ( 'NONE',  ( -54.55346411107571214, -23.96119346886879953, -0.6495511937832153526 ) ) ;
#79244=CARTESIAN_POINT ( 'NONE',  ( -110.6228709571500133, -24.52323809116983355, 9.355190652339425483 ) ) ;
#79248=EDGE_LOOP ( 'NONE', ( #81623, #14973, #94095, #72000 ) ) ;
#79249=CARTESIAN_POINT ( 'NONE',  ( -31.62287095715005236, -23.47596703998600276, 11.44779298504227505 ) ) ;
#79252=CARTESIAN_POINT ( 'NONE',  ( -13.01863806243235899, 16.06808769575019014, -1.500000000000002220 ) ) ;
#79253=ADVANCED_FACE ( 'NONE', ( #10793 ), #73201, .F. ) ;
#79254=CARTESIAN_POINT ( 'NONE',  ( 14.58690015069645263, 15.99052346098381250, 11.49999999999999645 ) ) ;
#79255=VERTEX_POINT ( 'NONE', #3689 ) ;
#79256=CARTESIAN_POINT ( 'NONE',  ( -98.93771941505393386, -25.28237778386645473, 5.756362269627500972 ) ) ;
#79257=CARTESIAN_POINT ( 'NONE',  ( -111.5960075431523251, -25.22279775002481017, 3.583730144309231758 ) ) ;
#79258=CARTESIAN_POINT ( 'NONE',  ( 11.21425909587273928, 19.38466839394011387, 11.49999999999998934 ) ) ;
#79259=CARTESIAN_POINT ( 'NONE',  ( -66.62287095715005592, -23.47596703998600276, 11.44779298504227683 ) ) ;
#79260=CARTESIAN_POINT ( 'NONE',  ( -120.6228709571500843, -24.51254535404255819, 9.355368623467654743 ) ) ;
#79261=EDGE_CURVE ( 'NONE', #20357, #80236, #77985, .T. ) ;
#79264=CARTESIAN_POINT ( 'NONE',  ( -35.63363566931067083, -24.73531770709095667, 8.716586749053508498 ) ) ;
#79265=EDGE_LOOP ( 'NONE', ( #72875, #17132, #90710, #7292 ) ) ;
#79266=ORIENTED_EDGE ( 'NONE', *, *, #48085, .T. ) ;
#79269=B_SPLINE_CURVE_WITH_KNOTS ( 'NONE', 3,
 ( #33298, #79478, #43791, #2875, #82341, #35679 ),
 .UNSPECIFIED., .F., .F.,
 ( 4, 2, 4 ),
 ( 6.384118678607784034E-06, 0.001386860460828371732, 0.002767336802978135387 ),
 .UNSPECIFIED. ) ;
#79270=ORIENTED_EDGE ( 'NONE', *, *, #70970, .T. ) ;
#79271=AXIS2_PLACEMENT_3D ( 'NONE', #61501, #8207, #39146 ) ;
#79273=FACE_OUTER_BOUND ( 'NONE', #26411, .T. ) ;
#79274=CARTESIAN_POINT ( 'NONE',  ( 0.06830352742921809439, -21.21198074455918814, -1.500000000000002220 ) ) ;
#79276=CARTESIAN_POINT ( 'NONE',  ( -50.52684846233325544, -24.92564183028979130, 1.928384488918255535 ) ) ;
#79277=CARTESIAN_POINT ( 'NONE',  ( -11.04117723084791614, -18.81814233335528286, -1.500000000000002220 ) ) ;
#79278=FACE_OUTER_BOUND ( 'NONE', #95367, .T. ) ;
#79280=CARTESIAN_POINT ( 'NONE',  ( -55.62287095715004170, -24.99132157543083821, 2.256160258750667502 ) ) ;
#79281=CARTESIAN_POINT ( 'NONE',  ( -1.606994170628035068, 21.82944698466814870, -1.500000000000002220 ) ) ;
#79282=CARTESIAN_POINT ( 'NONE',  ( -30.57287095715005520, -25.22658899513668729, 6.410055712259026706 ) ) ;
#79283=ORIENTED_EDGE ( 'NONE', *, *, #2836, .F. ) ;
#79287=VERTEX_POINT ( 'NONE', #44978 ) ;
#79288=B_SPLINE_CURVE_WITH_KNOTS ( 'NONE', 3,
 ( #57753, #58737, #90182, #66370, #34904, #65381 ),
 .UNSPECIFIED., .F., .F.,
 ( 4, 2, 4 ),
 ( 0.000000000000000000, 0.001380764517854768869, 0.002761529035709537738 ),
 .UNSPECIFIED. ) ;
#79290=CARTESIAN_POINT ( 'NONE',  ( -69.52287095715006160, -29.50250243563736774, 8.947779886222143375 ) ) ;
#79292=CARTESIAN_POINT ( 'NONE',  ( -21.21068194950259311, 0.7780057951688260642, -1.500000000000002220 ) ) ;
#79293=CARTESIAN_POINT ( 'NONE',  ( -44.62287095715004881, -23.48783264082478084, -1.443836473390072150 ) ) ;
#79294=CARTESIAN_POINT ( 'NONE',  ( -130.5728709571500588, -24.75991027412950274, 1.063373454495737391 ) ) ;
#79298=EDGE_CURVE ( 'NONE', #16500, #90746, #85363, .T. ) ;
#79299=CARTESIAN_POINT ( 'NONE',  ( 19.02374887324148389, -3.781047496429098764, -1.500000000000002220 ) ) ;
#79300=CARTESIAN_POINT ( 'NONE',  ( -45.58195093673430165, -24.73486907724917572, 1.287355809206967017 ) ) ;
#79301=ORIENTED_EDGE ( 'NONE', *, *, #99934, .T. ) ;
#79302=CARTESIAN_POINT ( 'NONE',  ( -11.52932745282126703, -15.74164922852205173, 11.49999999999999645 ) ) ;
#79303=CARTESIAN_POINT ( 'NONE',  ( -99.57255944844885676, -25.31502864763020355, 4.874549032268092219 ) ) ;
#79305=LINE ( 'NONE', #17416, #38270 ) ;
#79307=CARTESIAN_POINT ( 'NONE',  ( -93.62287095715001328, -24.33832256526969218, 0.1851278514119904517 ) ) ;
#79309=CARTESIAN_POINT ( 'NONE',  ( -89.60221604899453496, -23.48783264082478084, -1.443836473390068154 ) ) ;
#79311=EDGE_CURVE ( 'NONE', #54685, #60837, #78098, .T. ) ;
#79312=LINE ( 'NONE', #50381, #79591 ) ;
#79313=CARTESIAN_POINT ( 'NONE',  ( -81.52676753278062449, -25.03155964481168638, 7.119670603759651328 ) ) ;
#79314=CARTESIAN_POINT ( 'NONE',  ( -19.15281226579456231, 4.489446101945751444, 11.49999999999998934 ) ) ;
#79315=VECTOR ( 'NONE', #58178, 1000.000000000000114 ) ;
#79316=ORIENTED_EDGE ( 'NONE', *, *, #60765, .T. ) ;
#79317=VECTOR ( 'NONE', #21812, 1000.000000000000114 ) ;
#79319=CARTESIAN_POINT ( 'NONE',  ( 10.19088217375349892, 20.72639945755932800, -1.500000000000002220 ) ) ;
#79323=CARTESIAN_POINT ( 'NONE',  ( -90.52287095715001897, -24.82576562948886334, 8.398263436605496679 ) ) ;
#79324=CARTESIAN_POINT ( 'NONE',  ( -109.6313485239119672, -25.13840250613601413, 2.992668966235024541 ) ) ;
#79325=CARTESIAN_POINT ( 'NONE',  ( -97.63858573790135154, -23.48786465467241413, 11.44779295918254469 ) ) ;
#79329=CARTESIAN_POINT ( 'NONE',  ( -99.60745734687597519, -25.31566092335526008, 4.898549720458867718 ) ) ;
#79330=CARTESIAN_POINT ( 'NONE',  ( -8.676013072486071565, -17.92234406281952275, 11.49999999999998934 ) ) ;
#79332=CARTESIAN_POINT ( 'NONE',  ( -126.6228709571500559, -29.50250243563736774, 8.947779886222132717 ) ) ;
#79333=CARTESIAN_POINT ( 'NONE',  ( 19.84127317031322946, -0.4231496731191971561, -1.500000000000002220 ) ) ;
#79334=ORIENTED_EDGE ( 'NONE', *, *, #20269, .F. ) ;
#79335=PLANE ( 'NONE',  #47535 ) ;
#79338=CARTESIAN_POINT ( 'NONE',  ( -20.76960556195881225, -0.3855258213679747525, 11.49999999999999645 ) ) ;
#79339=DIRECTION ( 'NONE',  ( -3.773278334444167608E-23, 1.000000000000000000, 0.000000000000000000 ) ) ;
#79340=ADVANCED_FACE ( 'NONE', ( #4914 ), #34865, .F. ) ;
#79341=CARTESIAN_POINT ( 'NONE',  ( -106.5572847460906729, -23.73766607897671221, -1.055555164236449572 ) ) ;
#79342=CARTESIAN_POINT ( 'NONE',  ( 12.47407908559008760, -19.03963781694049473, 11.49999999999999645 ) ) ;
#79344=CARTESIAN_POINT ( 'NONE',  ( -69.49426968199877308, -24.65952944569304606, 1.056160979905704567 ) ) ;
#79345=EDGE_CURVE ( 'NONE', #39568, #31671, #68420, .T. ) ;
#79346=CARTESIAN_POINT ( 'NONE',  ( -100.5228709571500616, -25.00158670708909625, 2.256160236439166411 ) ) ;
#79347=VERTEX_POINT ( 'NONE', #28746 ) ;
#79348=CARTESIAN_POINT ( 'NONE',  ( -18.67835518149133378, -7.740158416121700746, 11.49999999999998934 ) ) ;
#79352=EDGE_CURVE ( 'NONE', #87739, #93213, #65836, .T. ) ;
#79353=ORIENTED_EDGE ( 'NONE', *, *, #35818, .F. ) ;
#79356=CARTESIAN_POINT ( 'NONE',  ( -16.75416981316412190, 10.96944243606782443, -1.500000000000002220 ) ) ;
#79357=CARTESIAN_POINT ( 'NONE',  ( -41.05437879045549465, -25.05917046252012170, 7.488404917370821146 ) ) ;
#79358=CARTESIAN_POINT ( 'NONE',  ( -16.25153318171239647, -13.25006309444557751, 11.49999999999999645 ) ) ;
#79359=DIRECTION ( 'NONE',  ( -3.773278334453080206E-23, 0.9999999999976377785, 2.173523156925979975E-06 ) ) ;
#79360=B_SPLINE_CURVE_WITH_KNOTS ( 'NONE', 3,
 ( #69637, #60036, #98568, #6722 ),
 .UNSPECIFIED., .F., .F.,
 ( 4, 4 ),
 ( 0.3507504623196067151, 0.3597568935917223043 ),
 .UNSPECIFIED. ) ;
#79362=CARTESIAN_POINT ( 'NONE',  ( 11.67614657018352453, 18.69773523334854914, -1.500000000000002220 ) ) ;
#79363=AXIS2_PLACEMENT_3D ( 'NONE', #33064, #54400, #47289 ) ;
#79366=CARTESIAN_POINT ( 'NONE',  ( -53.52287095715006870, -24.64898659630367916, 1.056161002820821038 ) ) ;
#79368=CARTESIAN_POINT ( 'NONE',  ( -72.56475442579929336, -23.48783264082477018, -1.443836473390095021 ) ) ;
#79370=FACE_OUTER_BOUND ( 'NONE', #96537, .T. ) ;
#79371=VERTEX_POINT ( 'NONE', #73925 ) ;
#79377=CARTESIAN_POINT ( 'NONE',  ( -19.23287947355762384, -7.152392467615741545, -1.500000000000002220 ) ) ;
#79379=CARTESIAN_POINT ( 'NONE',  ( -110.5562042904833930, -24.99156044556202971, 7.747789690856172307 ) ) ;
#79382=CARTESIAN_POINT ( 'NONE',  ( -46.62287095715004881, -23.47596703998600276, 11.44779298504227505 ) ) ;
#79383=CARTESIAN_POINT ( 'NONE',  ( 13.23790625878087468, -17.95846084735695314, 11.49999999999998934 ) ) ;
#79384=CARTESIAN_POINT ( 'NONE',  ( -71.30457154551150722, -25.25559839591754496, 6.209207386190694677 ) ) ;
#79387=EDGE_LOOP ( 'NONE', ( #100222, #4150, #63689, #43209 ) ) ;
#79392=CARTESIAN_POINT ( 'NONE',  ( -5.376107494350208960, -20.15860285114975525, -1.500000000000002220 ) ) ;
#79393=ORIENTED_EDGE ( 'NONE', *, *, #66531, .T. ) ;
#79394=CARTESIAN_POINT ( 'NONE',  ( -79.52287095715009002, -23.96177878511310055, 10.65340807706329862 ) ) ;
#79397=CARTESIAN_POINT ( 'NONE',  ( -69.79804103094413392, -25.03149351086992525, 7.463049324080706093 ) ) ;
#79398=CARTESIAN_POINT ( 'NONE',  ( 8.881738082190086203, 19.07353979602852689, -1.500000000000002220 ) ) ;
#79401=CARTESIAN_POINT ( 'NONE',  ( -114.6228709571500559, -29.50250786944525672, 11.44777988621622988 ) ) ;
#79402=CARTESIAN_POINT ( 'NONE',  ( -120.5166134144556764, -24.92592662359561473, 8.075495903018000021 ) ) ;
#79403=CARTESIAN_POINT ( 'NONE',  ( -86.63935476550661008, -23.73791477778911840, 11.05961554403170766 ) ) ;
#79404=CARTESIAN_POINT ( 'NONE',  ( -59.49371803394627278, -24.51314013834316441, 0.6176544820404136216 ) ) ;
#79405=CARTESIAN_POINT ( 'NONE',  ( -46.62287095715004881, -29.50248528299804818, 1.056150453629033370 ) ) ;
#79406=CARTESIAN_POINT ( 'NONE',  ( -73.62287095715005592, -29.50248528299804818, 1.056150453629036701 ) ) ;
#79407=CARTESIAN_POINT ( 'NONE',  ( -21.91529987491217923, -3.391794311424265018, 11.49999999999999645 ) ) ;
#79409=CARTESIAN_POINT ( 'NONE',  ( -109.5228709571500616, -23.47593901973090524, -1.443836447538996426 ) ) ;
#79410=DIRECTION ( 'NONE',  ( -3.773278334453079618E-23, 0.9999999999976377785, 2.173523156925979975E-06 ) ) ;
#79411=ORIENTED_EDGE ( 'NONE', *, *, #18664, .T. ) ;
#79412=CARTESIAN_POINT ( 'NONE',  ( -0.4833002549469566644, -22.66139224067150337, -1.500000000000002220 ) ) ;
#79415=ORIENTED_EDGE ( 'NONE', *, *, #96285, .F. ) ;
#79417=EDGE_CURVE ( 'NONE', #74266, #90387, #55127, .T. ) ;
#79418=CARTESIAN_POINT ( 'NONE',  ( 18.82035724208558491, -7.196742317222773799, -1.500000000000002220 ) ) ;
#79421=CARTESIAN_POINT ( 'NONE',  ( -130.5728709571500019, -24.56483619690598275, 0.5169519342574478982 ) ) ;
#79422=CARTESIAN_POINT ( 'NONE',  ( 6.968497804723354783, -21.30229754059623559, -1.500000000000002220 ) ) ;
#79423=B_SPLINE_CURVE_WITH_KNOTS ( 'NONE', 3,
 ( #33685, #87973, #80858, #3744 ),
 .UNSPECIFIED., .F., .F.,
 ( 4, 4 ),
 ( 0.2399572720920363500, 0.2489637033641517727 ),
 .UNSPECIFIED. ) ;
#79424=ORIENTED_EDGE ( 'NONE', *, *, #55304, .T. ) ;
#79426=CARTESIAN_POINT ( 'NONE',  ( -112.6245366205870795, -24.51419770103158413, 9.386484678747166299 ) ) ;
#79428=CARTESIAN_POINT ( 'NONE',  ( -96.62287095715005592, -23.47596703998600631, 11.44779298504227860 ) ) ;
#79429=EDGE_CURVE ( 'NONE', #62532, #39894, #58711, .T. ) ;
#79430=EDGE_CURVE ( 'NONE', #97480, #97261, #53595, .T. ) ;
#79433=CARTESIAN_POINT ( 'NONE',  ( -130.5728709571500019, -23.78062553189673167, -0.9709657327914282821 ) ) ;
#79434=CARTESIAN_POINT ( 'NONE',  ( -18.58057592369839384, -6.135153870360039896, -1.500000000000002220 ) ) ;
#79435=CARTESIAN_POINT ( 'NONE',  ( -59.62287095715004170, -24.65952944569304606, 1.056160979905694131 ) ) ;
#79438=CARTESIAN_POINT ( 'NONE',  ( 5.543860000110784725, 20.76261553274053284, -1.500000000000002220 ) ) ;
#79439=CARTESIAN_POINT ( 'NONE',  ( -102.6228709571500417, -23.48786465467241769, 11.44779295918253936 ) ) ;
#79441=LINE ( 'NONE', #25659, #14998 ) ;
#79443=CARTESIAN_POINT ( 'NONE',  ( -77.62287095715007013, -24.66019654487199730, 8.947790411086128159 ) ) ;
#79444=CARTESIAN_POINT ( 'NONE',  ( -14.16064136294604303, -18.02537036913223290, -1.500000000000002220 ) ) ;
#79445=B_SPLINE_CURVE_WITH_KNOTS ( 'NONE', 3,
 ( #37234, #62075, #84894, #22479, #75283, #21983, #15375, #68185, #7773, #52463, #91504, #45845, #77269, #67701 ),
 .UNSPECIFIED., .F., .F.,
 ( 4, 2, 2, 2, 2, 2, 4 ),
 ( 0.000000000000000000, 0.0002247388865718425940, 0.0004494777731436851880, 0.0008989555462873846875, 0.001348433319431084241, 0.001573172206002952395, 0.001797911092574820549 ),
 .UNSPECIFIED. ) ;
#79447=CARTESIAN_POINT ( 'NONE',  ( -39.62287095715004881, -23.48783264082477373, -1.443836473390072594 ) ) ;
#79448=CARTESIAN_POINT ( 'NONE',  ( -53.64457316383079899, -23.96119346886879953, -0.6495511937832126881 ) ) ;
#79449=CARTESIAN_POINT ( 'NONE',  ( -16.19606052442943067, -11.93128464602566474, 11.49999999999999645 ) ) ;
#79451=CARTESIAN_POINT ( 'NONE',  ( -113.6228709571500559, -24.64965695001469115, 8.947790433994176951 ) ) ;
#79452=CARTESIAN_POINT ( 'NONE',  ( -99.52287095715009002, -23.96127896942179092, -0.6493128930930167630 ) ) ;
#79453=CARTESIAN_POINT ( 'NONE',  ( -89.52287095715006160, -29.50250243563736774, 8.947779886222139822 ) ) ;
#79454=CARTESIAN_POINT ( 'NONE',  ( -109.5228709571500616, -23.47593901973090524, -1.443836447538996426 ) ) ;
#79455=CARTESIAN_POINT ( 'NONE',  ( -12.90690225449951001, 15.05119527412115055, 11.49999999999998934 ) ) ;
#79457=CARTESIAN_POINT ( 'NONE',  ( 0.2638585030419089428, -21.76204025362994798, 11.49999999999998934 ) ) ;
#79459=CARTESIAN_POINT ( 'NONE',  ( 9.307004028210867475, 17.29072351678862418, -1.500000000000002220 ) ) ;
#79463=CARTESIAN_POINT ( 'NONE',  ( -54.52287095715006160, -23.96177878511308279, 10.65340807706330217 ) ) ;
#79466=CARTESIAN_POINT ( 'NONE',  ( -115.6228709571500559, -24.62226745350443835, 0.9660975649729570680 ) ) ;
#79468=CARTESIAN_POINT ( 'NONE',  ( 20.13950599927006735, 4.067174238878714654, 11.49999999999999645 ) ) ;
#79470=EDGE_CURVE ( 'NONE', #53498, #38852, #95004, .T. ) ;
#79471=CARTESIAN_POINT ( 'NONE',  ( -128.5228709571500758, -24.35013146730205236, 9.818937971375092388 ) ) ;
#79472=CARTESIAN_POINT ( 'NONE',  ( 5.419076944403256491, 21.93356404788375258, 11.49999999999999645 ) ) ;
#79473=EDGE_LOOP ( 'NONE', ( #48620, #76727, #59060, #54426 ) ) ;
#79475=CARTESIAN_POINT ( 'NONE',  ( -99.93377387090225739, -25.26387419355090103, 4.577608625778666784 ) ) ;
#79477=CARTESIAN_POINT ( 'NONE',  ( -50.49617078905069434, -25.31259386660232380, 4.732512649054961607 ) ) ;
#79478=CARTESIAN_POINT ( 'NONE',  ( -64.52287095715006160, -23.73907113216989728, -1.053371485793254791 ) ) ;
#79479=CARTESIAN_POINT ( 'NONE',  ( -110.6228709571500843, -23.47596703998600631, 11.44779298504227860 ) ) ;
#79480=EDGE_CURVE ( 'NONE', #9517, #31838, #85013, .T. ) ;
#79482=ADVANCED_FACE ( 'NONE', ( #31737 ), #38844, .T. ) ;
#79483=B_SPLINE_CURVE_WITH_KNOTS ( 'NONE', 3,
 ( #55391, #47274, #69095, #15808 ),
 .UNSPECIFIED., .F., .F.,
 ( 4, 4 ),
 ( 0.000000000000000000, 9.999999999998900014E-05 ),
 .UNSPECIFIED. ) ;
#79484=ORIENTED_EDGE ( 'NONE', *, *, #99393, .T. ) ;
#79485=CARTESIAN_POINT ( 'NONE',  ( -79.57226238056755108, -25.26749951328133648, 5.312439035903004481 ) ) ;
#79486=CARTESIAN_POINT ( 'NONE',  ( -19.58686714514938387, 11.73587220785771379, -1.500000000000002220 ) ) ;
#79489=CARTESIAN_POINT ( 'NONE',  ( -82.54406659160568438, -24.51419770103156281, 9.386484678747185839 ) ) ;
#79490=CARTESIAN_POINT ( 'NONE',  ( 22.08653571170524543, -4.319401766784854324, 11.49999999999999645 ) ) ;
#79491=ORIENTED_EDGE ( 'NONE', *, *, #97220, .F. ) ;
#79492=CARTESIAN_POINT ( 'NONE',  ( -43.62864466859128498, -24.51314013834316086, 0.6176544820404145097 ) ) ;
#79493=CARTESIAN_POINT ( 'NONE',  ( -21.26704322615652032, -5.532269525099344776, -1.500000000000002220 ) ) ;
#79494=DIRECTION ( 'NONE',  ( 1.000000000000000000, 3.773278334444166432E-23, 8.201307841325785021E-29 ) ) ;
#79496=CARTESIAN_POINT ( 'NONE',  ( -69.47536397586432599, -25.08820418785056106, 7.294817312633749218 ) ) ;
#79497=ORIENTED_EDGE ( 'NONE', *, *, #58304, .T. ) ;
#79498=CARTESIAN_POINT ( 'NONE',  ( -106.6228709571500559, -29.50247984919015209, -1.443849546365048253 ) ) ;
#79501=CARTESIAN_POINT ( 'NONE',  ( 19.18951349294833264, 7.196795126939715459, 11.49999999999998934 ) ) ;
#79503=VERTEX_POINT ( 'NONE', #38346 ) ;
#79504=ORIENTED_EDGE ( 'NONE', *, *, #32957, .F. ) ;
#79505=ORIENTED_EDGE ( 'NONE', *, *, #50259, .T. ) ;
#79506=CARTESIAN_POINT ( 'NONE',  ( -84.62287095715001328, -23.73907113216990439, -1.053371485793225704 ) ) ;
#79507=CARTESIAN_POINT ( 'NONE',  ( 6.977686149863070675, -22.03694335537135984, -1.500000000000002220 ) ) ;
#79508=CARTESIAN_POINT ( 'NONE',  ( -41.52287095715009002, -23.96177878511308279, 10.65340807706330573 ) ) ;
#79509=CARTESIAN_POINT ( 'NONE',  ( -9.641467040090685003, 17.89903724589931855, -1.500000000000002220 ) ) ;
#79512=CARTESIAN_POINT ( 'NONE',  ( -92.58855986348115152, -24.34968618360935011, 0.1864209137778965741 ) ) ;
#79513=CARTESIAN_POINT ( 'NONE',  ( -114.6228709571500701, -23.96177878511308634, 10.65340807706329862 ) ) ;
#79515=CARTESIAN_POINT ( 'NONE',  ( -21.39523464106120088, -1.845724655749456433, 11.49999999999999645 ) ) ;
#79516=VERTEX_POINT ( 'NONE', #93123 ) ;
#79520=CARTESIAN_POINT ( 'NONE',  ( -1.268444833121266546, 20.69640364028325052, -1.500000000000002220 ) ) ;
#79521=VECTOR ( 'NONE', #51085, 1000.000000000000114 ) ;
#79522=ORIENTED_EDGE ( 'NONE', *, *, #39127, .T. ) ;
#79523=CARTESIAN_POINT ( 'NONE',  ( -125.5909827109052941, -23.85016227208582151, -0.8807180028928047744 ) ) ;
#79524=EDGE_LOOP ( 'NONE', ( #55077, #64526, #43534, #46074 ) ) ;
#79525=PLANE ( 'NONE',  #39028 ) ;
#79526=CARTESIAN_POINT ( 'NONE',  ( -107.6228709571500559, -24.50216790748098461, 0.6166512839513795807 ) ) ;
#79527=ORIENTED_EDGE ( 'NONE', *, *, #95286, .F. ) ;
#79528=ORIENTED_EDGE ( 'NONE', *, *, #36432, .F. ) ;
#79529=CARTESIAN_POINT ( 'NONE',  ( -40.52287095715006870, -24.92579138211019085, 1.929029949965664015 ) ) ;
#79530=B_SPLINE_CURVE_WITH_KNOTS ( 'NONE', 3,
 ( #95929, #57395, #88323, #11195 ),
 .UNSPECIFIED., .F., .F.,
 ( 4, 4 ),
 ( 0.4090588724279532462, 0.4100596194687187723 ),
 .UNSPECIFIED. ) ;
#79531=B_SPLINE_CURVE_WITH_KNOTS ( 'NONE', 3,
 ( #72291, #16985, #15978, #77873, #78873, #39324, #31719, #16478 ),
 .UNSPECIFIED., .F., .F.,
 ( 4, 2, 2, 4 ),
 ( 6.391158118961346620E-06, 0.002007136338672917911, 0.003007508928949897790, 0.004007881519226878103 ),
 .UNSPECIFIED. ) ;
#79533=CARTESIAN_POINT ( 'NONE',  ( -29.03431458974025148, -24.86372088895192789, 2.176981720316843116 ) ) ;
#79534=CARTESIAN_POINT ( 'NONE',  ( -18.24146354680218707, 12.35505607031776165, 11.49999999999999645 ) ) ;
#79536=CARTESIAN_POINT ( 'NONE',  ( -103.5600735941376485, -23.48783264082477018, -1.443836473390091246 ) ) ;
#79537=CARTESIAN_POINT ( 'NONE',  ( -19.94007547503736788, -10.58355046294204094, -1.500000000000002220 ) ) ;
#79542=AXIS2_PLACEMENT_3D ( 'NONE', #86620, #9496, #54191 ) ;
#79543=CARTESIAN_POINT ( 'NONE',  ( -88.52287095715004739, -23.96177878511308634, 10.65340807706329329 ) ) ;
#79544=CARTESIAN_POINT ( 'NONE',  ( -128.6228709571500417, -23.48783264082479505, -1.443836473390056829 ) ) ;
#79546=CARTESIAN_POINT ( 'NONE',  ( 4.565063516603933280, 20.63981631578574039, 11.49999999999998934 ) ) ;
#79547=DIRECTION ( 'NONE',  ( 0.000000000000000000, -0.9999999999976377785, -2.173523156925979128E-06 ) ) ;
#79549=CARTESIAN_POINT ( 'NONE',  ( -51.71530383401179876, -25.03148599924218232, 6.909342695069468299 ) ) ;
#79552=CARTESIAN_POINT ( 'NONE',  ( -14.87450875942801254, -16.50811611944624602, -1.500000000000002220 ) ) ;
#79553=EDGE_CURVE ( 'NONE', #82501, #56235, #7836, .T. ) ;
#79554=CARTESIAN_POINT ( 'NONE',  ( -114.5568548638380264, -23.73766607897672287, -1.055555164236428700 ) ) ;
#79556=VERTEX_POINT ( 'NONE', #86020 ) ;
#79557=DIRECTION ( 'NONE',  ( -3.773278334453079030E-23, 0.9999999999976377785, 2.173523156925979128E-06 ) ) ;
#79558=LINE ( 'NONE', #33378, #18443 ) ;
#79559=CARTESIAN_POINT ( 'NONE',  ( -13.55963120218723361, -13.89248740512243430, 11.49999999999999645 ) ) ;
#79560=EDGE_CURVE ( 'NONE', #39568, #60922, #85514, .T. ) ;
#79561=EDGE_CURVE ( 'NONE', #56711, #85538, #61702, .T. ) ;
#79562=CARTESIAN_POINT ( 'NONE',  ( -40.53071971990141975, -25.11095176003700757, 2.835807588750839603 ) ) ;
#79563=CARTESIAN_POINT ( 'NONE',  ( -33.62287095715003460, -23.95044443724991368, 10.65354141964649948 ) ) ;
#79564=CARTESIAN_POINT ( 'NONE',  ( -19.44331071757236273, 1.017868325215548708, -1.500000000000002220 ) ) ;
#79565=CARTESIAN_POINT ( 'NONE',  ( -19.74196057798672399, -8.316236533413031040, -1.500000000000002220 ) ) ;
#79567=CARTESIAN_POINT ( 'NONE',  ( -60.53292233517615273, -24.83644354574317603, 8.397322867105112110 ) ) ;
#79568=CARTESIAN_POINT ( 'NONE',  ( -100.6228709571500701, -24.63345952396256067, 9.038047939301499412 ) ) ;
#79569=CARTESIAN_POINT ( 'NONE',  ( -101.6228709571500559, -24.64965695001469115, 8.947790433994178727 ) ) ;
#79570=CARTESIAN_POINT ( 'NONE',  ( 16.28376985728763415, 15.88423345705086298, -1.500000000000002220 ) ) ;
#79572=CARTESIAN_POINT ( 'NONE',  ( -98.62537220214177580, -24.51314013834316086, 0.6176544820404117342 ) ) ;
#79573=CARTESIAN_POINT ( 'NONE',  ( -98.62287095715005592, -23.48783264082478439, -1.443836473390061936 ) ) ;
#79574=CARTESIAN_POINT ( 'NONE',  ( 5.644138345009856117, 19.01542066204735448, 11.49999999999999645 ) ) ;
#79575=CARTESIAN_POINT ( 'NONE',  ( -69.52287095715009002, -23.48783264082477018, -1.443836473390092801 ) ) ;
#79576=LINE ( 'NONE', #87696, #71696 ) ;
#79577=CARTESIAN_POINT ( 'NONE',  ( -48.66104112521659886, -23.48783264082477729, -1.443836473390069486 ) ) ;
#79578=ORIENTED_EDGE ( 'NONE', *, *, #6598, .T. ) ;
#79580=EDGE_CURVE ( 'NONE', #7329, #74994, #70305, .T. ) ;
#79581=FACE_OUTER_BOUND ( 'NONE', #89782, .T. ) ;
#79582=CARTESIAN_POINT ( 'NONE',  ( -75.52287095715006160, -24.99132157543084176, 2.256160258750667502 ) ) ;
#79583=CARTESIAN_POINT ( 'NONE',  ( -17.53059066697263546, 12.75712217820542627, 11.49999999999998934 ) ) ;
#79584=CARTESIAN_POINT ( 'NONE',  ( -56.54791891829369632, -24.15620529776628445, 10.23563542870660648 ) ) ;
#79585=CARTESIAN_POINT ( 'NONE',  ( 16.17817332762582794, -10.88531698672339942, -1.500000000000002220 ) ) ;
#79587=ADVANCED_FACE ( 'NONE', ( #99238 ), #39428, .T. ) ;
#79588=ORIENTED_EDGE ( 'NONE', *, *, #24806, .T. ) ;
#79589=CARTESIAN_POINT ( 'NONE',  ( -13.80512455850298714, -15.04058748057734896, 11.49999999999999645 ) ) ;
#79591=VECTOR ( 'NONE', #18912, 1000.000000000000114 ) ;
#79594=CARTESIAN_POINT ( 'NONE',  ( -80.30096212672883382, -25.03465771498776959, 7.554806159496210149 ) ) ;
#79595=DIRECTION ( 'NONE',  ( 1.000000000000000000, 3.773278334444167608E-23, 8.201307833595939069E-29 ) ) ;
#79596=CARTESIAN_POINT ( 'NONE',  ( -125.5228709571500616, -24.99156044556120904, 7.747789690856173195 ) ) ;
#79597=CARTESIAN_POINT ( 'NONE',  ( -49.45828852499023753, -25.31439371758138890, 5.632644884985086975 ) ) ;
#79602=ADVANCED_FACE ( 'NONE', ( #3314 ), #70212, .T. ) ;
#79603=VECTOR ( 'NONE', #18049, 1000.000000000000114 ) ;
#79604=CARTESIAN_POINT ( 'NONE',  ( 4.748521865011817944, 22.44708532425888592, 11.49999999999999645 ) ) ;
#79605=CARTESIAN_POINT ( 'NONE',  ( 16.28376985728763415, 15.88423345705086298, 11.49999999999998934 ) ) ;
#79606=CARTESIAN_POINT ( 'NONE',  ( -110.5886784188881506, -24.63419186844610920, 9.035850630976920428 ) ) ;
#79608=CARTESIAN_POINT ( 'NONE',  ( -90.50427414553793426, -24.63355581998384736, 0.9682620441943978751 ) ) ;
#79611=CARTESIAN_POINT ( 'NONE',  ( -17.40403014803320758, -13.24600170205644289, 11.49999999999998934 ) ) ;
#79612=CARTESIAN_POINT ( 'NONE',  ( -69.56521275654560554, -23.48786465467240347, 11.44779295918255002 ) ) ;
#79613=CARTESIAN_POINT ( 'NONE',  ( -27.53894643728430580, -24.76187901197181773, 2.282776568623821500 ) ) ;
#79615=CARTESIAN_POINT ( 'NONE',  ( -98.92944106970213625, -25.31200674615046253, 5.790834157640309066 ) ) ;
#79617=CARTESIAN_POINT ( 'NONE',  ( -19.95082702767638239, -4.354873812894156870, 11.49999999999998934 ) ) ;
#79618=EDGE_LOOP ( 'NONE', ( #18129, #8774, #99933, #95968 ) ) ;
#79620=CARTESIAN_POINT ( 'NONE',  ( -23.02147672596084149, 0.6323230698326208765, -1.500000000000002220 ) ) ;
#79622=ORIENTED_EDGE ( 'NONE', *, *, #89286, .T. ) ;
#79623=CARTESIAN_POINT ( 'NONE',  ( -110.6167769405262362, -25.21876678810425076, 6.586934760171002878 ) ) ;
#79624=CARTESIAN_POINT ( 'NONE',  ( -32.62287095715004881, -24.65952944569304250, 1.056160979905691688 ) ) ;
#79627=CARTESIAN_POINT ( 'NONE',  ( 13.65650298889772962, 16.33668418983593185, 11.49999999999999645 ) ) ;
#79630=CARTESIAN_POINT ( 'NONE',  ( -21.98633505697190671, -3.258044352128648846, -1.500000000000002220 ) ) ;
#79631=CARTESIAN_POINT ( 'NONE',  ( 3.034461355793923509, -20.43525710956717845, -1.500000000000002220 ) ) ;
#79632=VERTEX_POINT ( 'NONE', #19004 ) ;
#79633=DIRECTION ( 'NONE',  ( 1.000000000000000000, 3.773278334444166432E-23, 8.201307841325785021E-29 ) ) ;
#79634=CARTESIAN_POINT ( 'NONE',  ( -95.62858372876527824, -24.63419186844610920, 9.035850630976922204 ) ) ;
#79636=DIRECTION ( 'NONE',  ( -3.773278334453079030E-23, 0.9999999999976377785, 2.173523156925979128E-06 ) ) ;
#79637=ORIENTED_EDGE ( 'NONE', *, *, #74730, .T. ) ;
#79640=CARTESIAN_POINT ( 'NONE',  ( 20.66465755290784401, -3.126920214821775623, -1.500000000000002220 ) ) ;
#79641=CARTESIAN_POINT ( 'NONE',  ( -16.21501377034323710, -14.60173171477820198, 11.49999999999999645 ) ) ;
#79642=CARTESIAN_POINT ( 'NONE',  ( -26.56775203954515874, -24.77993665650937061, 6.997625439131231140 ) ) ;
#79644=CARTESIAN_POINT ( 'NONE',  ( 3.433349652534986696, 22.22849440524942111, -1.500000000000002220 ) ) ;
#79645=CARTESIAN_POINT ( 'NONE',  ( 0.8369575198195864374, -20.89415947959451003, -1.500000000000002220 ) ) ;
#79646=CARTESIAN_POINT ( 'NONE',  ( -26.33488822642538452, -24.88149058068788122, 6.524121877972378414 ) ) ;
#79647=CARTESIAN_POINT ( 'NONE',  ( -52.52287095715008292, -24.66019654487198665, 8.947790411086131712 ) ) ;
#79650=VERTEX_POINT ( 'NONE', #35243 ) ;
#79651=VERTEX_POINT ( 'NONE', #90022 ) ;
#79653=CARTESIAN_POINT ( 'NONE',  ( -52.65162834406839920, -23.73766607897671221, -1.055555164236436472 ) ) ;
#79654=VERTEX_POINT ( 'NONE', #36732 ) ;
#79655=B_SPLINE_CURVE_WITH_KNOTS ( 'NONE', 3,
 ( #21936, #55811, #71530, #53419, #87236, #71027 ),
 .UNSPECIFIED., .F., .F.,
 ( 4, 2, 4 ),
 ( 0.000000000000000000, 0.001380764517854766700, 0.002761529035709533401 ),
 .UNSPECIFIED. ) ;
#79656=CARTESIAN_POINT ( 'NONE',  ( -4.378498130703003532, 20.98420022172975763, -1.500000000000002220 ) ) ;
#79657=CARTESIAN_POINT ( 'NONE',  ( 22.34790896907852442, -0.4833156648990815651, 11.49999999999999645 ) ) ;
#79660=CARTESIAN_POINT ( 'NONE',  ( 5.245434476726341444, -20.39595507048906242, -1.500000000000002220 ) ) ;
#79661=CARTESIAN_POINT ( 'NONE',  ( -30.49162772548749700, -24.48101848413686099, 9.440108529385041081 ) ) ;
#79662=EDGE_CURVE ( 'NONE', #80731, #55399, #28128, .T. ) ;
#79663=CARTESIAN_POINT ( 'NONE',  ( -16.79965634883036074, 10.71410036745690597, -1.500000000000002220 ) ) ;
#79664=CARTESIAN_POINT ( 'NONE',  ( -50.57647688411456244, -24.92592662359560762, 8.075495903017996469 ) ) ;
#79666=CARTESIAN_POINT ( 'NONE',  ( 17.21905055353458991, -13.78536315820828229, -1.500000000000002220 ) ) ;
#79668=FACE_OUTER_BOUND ( 'NONE', #100056, .T. ) ;
#79671=CARTESIAN_POINT ( 'NONE',  ( 19.93353245626563819, -6.116835970281883306, 11.49999999999999645 ) ) ;
#79673=CARTESIAN_POINT ( 'NONE',  ( -25.52552615364072253, -24.47148205344575800, 8.290116722409051064 ) ) ;
#79674=AXIS2_PLACEMENT_3D ( 'NONE', #66129, #67117, #52876 ) ;
#79675=EDGE_CURVE ( 'NONE', #59182, #4570, #39286, .T. ) ;
#79676=DIRECTION ( 'NONE',  ( -3.773278334453079618E-23, 0.9999999999976377785, 2.173523156925979975E-06 ) ) ;
#79679=CARTESIAN_POINT ( 'NONE',  ( 1.434216325579209750, -21.26356369375713484, -1.500000000000002220 ) ) ;
#79681=ADVANCED_FACE ( 'NONE', ( #66213 ), #51466, .F. ) ;
#79684=CARTESIAN_POINT ( 'NONE',  ( -68.62287095715005592, -23.48783264082478439, -1.443836473390067265 ) ) ;
#79685=CARTESIAN_POINT ( 'NONE',  ( -18.09186581907994196, -13.49991075323410250, -1.500000000000002220 ) ) ;
#79686=CARTESIAN_POINT ( 'NONE',  ( -51.52287095715004739, -23.73934037231757088, 11.05740245334329508 ) ) ;
#79687=ORIENTED_EDGE ( 'NONE', *, *, #42932, .F. ) ;
#79689=CARTESIAN_POINT ( 'NONE',  ( -31.53139797621515328, -24.51419770103156637, 9.386484678747187615 ) ) ;
#79690=CARTESIAN_POINT ( 'NONE',  ( -0.8432318219891272726, -19.69000482574202238, 11.49999999999999645 ) ) ;
#79691=CARTESIAN_POINT ( 'NONE',  ( -32.07722060962683486, -25.26313220207395105, 6.450164452698709638 ) ) ;
#79694=ORIENTED_EDGE ( 'NONE', *, *, #80711, .F. ) ;
#79695=PLANE ( 'NONE',  #86267 ) ;
#79696=CARTESIAN_POINT ( 'NONE',  ( -127.4728709594060092, -25.21147767388033500, 8.000950760261464012 ) ) ;
#79697=CARTESIAN_POINT ( 'NONE',  ( -61.52287095715008292, -24.51387760970724727, 9.387446482453409402 ) ) ;
#79698=DIRECTION ( 'NONE',  ( 3.773278334444166432E-23, -1.000000000000000000, 0.000000000000000000 ) ) ;
#79700=EDGE_CURVE ( 'NONE', #88020, #95160, #22380, .T. ) ;
#79701=CARTESIAN_POINT ( 'NONE',  ( -60.62287095715004881, -23.47593901973091235, -1.443836447539007972 ) ) ;
#79702=CARTESIAN_POINT ( 'NONE',  ( -15.39140670439391378, -12.39996395878027791, -1.500000000000002220 ) ) ;
#79703=ORIENTED_EDGE ( 'NONE', *, *, #15418, .T. ) ;
#79704=CARTESIAN_POINT ( 'NONE',  ( -2.479824388263708990, 20.08073137130260122, 11.49999999999999645 ) ) ;
#79707=B_SPLINE_CURVE_WITH_KNOTS ( 'NONE', 3,
 ( #57286, #11573, #43539, #49660, #51144, #74476 ),
 .UNSPECIFIED., .F., .F.,
 ( 4, 2, 4 ),
 ( 0.000000000000000000, 0.001380901958385382473, 0.002761803916770764946 ),
 .UNSPECIFIED. ) ;
#79709=CARTESIAN_POINT ( 'NONE',  ( -40.52287095715006870, -23.47593901973090169, -1.443836447538997092 ) ) ;
#79712=CARTESIAN_POINT ( 'NONE',  ( -69.65500006739829075, -25.13901286917058187, 2.995211960630785430 ) ) ;
#79713=PLANE ( 'NONE',  #52217 ) ;
#79714=CARTESIAN_POINT ( 'NONE',  ( -57.52287095715005449, -29.50247984919015209, -1.443849546365056913 ) ) ;
#79715=CARTESIAN_POINT ( 'NONE',  ( -7.547287378330592489, -18.53391252851691462, 11.49999999999998934 ) ) ;
#79716=EDGE_CURVE ( 'NONE', #27769, #59549, #62317, .T. ) ;
#79717=CARTESIAN_POINT ( 'NONE',  ( -99.16315266720698673, -25.27533051753978910, 3.707282223935987275 ) ) ;
#79718=ORIENTED_EDGE ( 'NONE', *, *, #58045, .F. ) ;
#79720=FACE_OUTER_BOUND ( 'NONE', #74052, .T. ) ;
#79721=DIRECTION ( 'NONE',  ( -3.773278334453079618E-23, 0.9999999999976377785, 2.173523156925979975E-06 ) ) ;
#79724=CARTESIAN_POINT ( 'NONE',  ( -73.58111945615931404, -24.65952944569304606, 1.056160979905700126 ) ) ;
#79726=ADVANCED_FACE ( 'NONE', ( #81909 ), #84764, .T. ) ;
#79727=CARTESIAN_POINT ( 'NONE',  ( -99.90536206787731999, -25.32724633150700200, 4.398074151685131383 ) ) ;
#79730=CARTESIAN_POINT ( 'NONE',  ( 17.43904876784772284, 10.37648870149486413, -1.500000000000002220 ) ) ;
#79734=CARTESIAN_POINT ( 'NONE',  ( -127.5561563095140798, -23.73791477778912551, 11.05961554403169167 ) ) ;
#79735=CARTESIAN_POINT ( 'NONE',  ( -59.54286866093478636, -24.35071581493543391, 9.817618358456035921 ) ) ;
#79738=CARTESIAN_POINT ( 'NONE',  ( -30.47287095715006799, -25.25852548890106419, 3.876286009398770993 ) ) ;
#79739=CARTESIAN_POINT ( 'NONE',  ( -18.51692787870624102, -10.26217664800131502, 11.49999999999999645 ) ) ;
#79741=CARTESIAN_POINT ( 'NONE',  ( -20.57447749561850969, 8.151157241358404804, 11.49999999999998934 ) ) ;
#79742=B_SPLINE_CURVE_WITH_KNOTS ( 'NONE', 3,
 ( #66720, #44859, #52468, #83400, #28134, #12393, #37729, #75288 ),
 .UNSPECIFIED., .F., .F.,
 ( 4, 2, 2, 4 ),
 ( -0.001224873891641424777, -0.0002244903592271093630, 0.0007758931731872060512, 0.002776660238015836880 ),
 .UNSPECIFIED. ) ;
#79743=B_SPLINE_CURVE_WITH_KNOTS ( 'NONE', 3,
 ( #76883, #38343, #29768, #53621 ),
 .UNSPECIFIED., .F., .F.,
 ( 4, 4 ),
 ( 0.000000000000000000, 9.999999999998897304E-05 ),
 .UNSPECIFIED. ) ;
#79745=CARTESIAN_POINT ( 'NONE',  ( 9.245221688665949955, -18.36014492602614467, 11.49999999999998934 ) ) ;
#79748=EDGE_LOOP ( 'NONE', ( #47837, #96966, #71302, #86732 ) ) ;
#79749=CARTESIAN_POINT ( 'NONE',  ( -37.52287095715006870, -23.47596703998600631, 11.44779298504229281 ) ) ;
#79753=ORIENTED_EDGE ( 'NONE', *, *, #36061, .F. ) ;
#79757=CARTESIAN_POINT ( 'NONE',  ( 4.478411676025833010, -20.21887007069289766, -1.500000000000002220 ) ) ;
#79758=CARTESIAN_POINT ( 'NONE',  ( -15.38093110518717666, 15.28219592669002402, 11.49999999999999645 ) ) ;
#79759=VERTEX_POINT ( 'NONE', #15374 ) ;
#79760=CARTESIAN_POINT ( 'NONE',  ( -60.52287095715006870, -23.85229601349281126, 10.88205029485767561 ) ) ;
#79761=DIRECTION ( 'NONE',  ( -3.773278334453079030E-23, 0.9999999999976377785, 2.173523156925979128E-06 ) ) ;
#79762=CARTESIAN_POINT ( 'NONE',  ( 22.03792223356247604, -4.036589945906135846, -1.500000000000002220 ) ) ;
#79764=LINE ( 'NONE', #11752, #69196 ) ;
#79765=VERTEX_POINT ( 'NONE', #62074 ) ;
#79770=ORIENTED_EDGE ( 'NONE', *, *, #90605, .T. ) ;
#79772=VERTEX_POINT ( 'NONE', #52963 ) ;
#79774=CARTESIAN_POINT ( 'NONE',  ( 5.514125806255895004E-17, -29.50247984919086264, -1.443849221408822103 ) ) ;
#79775=CARTESIAN_POINT ( 'NONE',  ( 4.782327729912362990, -20.71560727227588927, -1.500000000000002220 ) ) ;
#79778=CARTESIAN_POINT ( 'NONE',  ( -13.95179422449595208, 16.79422078803934326, -1.500000000000002220 ) ) ;
#79779=CARTESIAN_POINT ( 'NONE',  ( -103.5856489833065410, -24.66019654487200086, 8.947790411086119278 ) ) ;
#79780=LINE ( 'NONE', #18389, #22593 ) ;
#79781=CARTESIAN_POINT ( 'NONE',  ( -109.6228709571500417, -24.65952944569305316, 1.056160979905704345 ) ) ;
#79782=CARTESIAN_POINT ( 'NONE',  ( 6.672210613628693388, 20.84999943921648935, -1.500000000000002220 ) ) ;
#79784=ORIENTED_EDGE ( 'NONE', *, *, #47429, .T. ) ;
#79786=CARTESIAN_POINT ( 'NONE',  ( -48.87380231474225667, -25.26337302231874915, 6.137091984676827039 ) ) ;
#79790=VECTOR ( 'NONE', #100262, 1000.000000000000114 ) ;
#79791=EDGE_CURVE ( 'NONE', #52807, #37472, #57469, .T. ) ;
#79792=CARTESIAN_POINT ( 'NONE',  ( -29.05897231630594035, -25.07799921448866343, 3.365375995075712279 ) ) ;
#79793=CARTESIAN_POINT ( 'NONE',  ( -80.52287095715006160, -23.47593901973090169, -1.443836447538996648 ) ) ;
#79794=CARTESIAN_POINT ( 'NONE',  ( -21.21068194950259311, 0.7780057951688260642, 11.49999999999998934 ) ) ;
#79795=CARTESIAN_POINT ( 'NONE',  ( -91.62287095715004170, -29.50248528299804818, 1.056150453629040253 ) ) ;
#79796=EDGE_CURVE ( 'NONE', #99590, #10228, #76830, .T. ) ;
#79797=CARTESIAN_POINT ( 'NONE',  ( -30.64427850938830744, -23.56000036390796382, 11.50200000000000067 ) ) ;
#79798=PLANE ( 'NONE',  #14569 ) ;
#79799=CARTESIAN_POINT ( 'NONE',  ( -127.5562042904833930, -24.66019654487200441, 8.947790411086121054 ) ) ;
#79800=CARTESIAN_POINT ( 'NONE',  ( -16.37229413335033001, -10.43475415037859655, -1.500000000000002220 ) ) ;
#79801=CARTESIAN_POINT ( 'NONE',  ( -117.6242398451807389, -24.51419770103158768, 9.386484678747164523 ) ) ;
#79803=CARTESIAN_POINT ( 'NONE',  ( 10.93668938013857783, -16.14717738681254033, 11.49999999999999645 ) ) ;
#79807=ORIENTED_EDGE ( 'NONE', *, *, #30242, .F. ) ;
#79809=CARTESIAN_POINT ( 'NONE',  ( -89.54348968983181578, -24.65952944569304250, 1.056160979905700126 ) ) ;
#79811=VECTOR ( 'NONE', #74094, 1000.000000000000114 ) ;
#79812=CARTESIAN_POINT ( 'NONE',  ( -81.88534077628074215, -25.24813715446843432, 6.293942979331170307 ) ) ;
#79813=CARTESIAN_POINT ( 'NONE',  ( -8.025172913017740939, -17.94849717234452768, -1.500000000000002220 ) ) ;
#79815=ORIENTED_EDGE ( 'NONE', *, *, #30190, .F. ) ;
#79817=CARTESIAN_POINT ( 'NONE',  ( -20.32320236877023589, 10.94715076914730290, -1.500000000000002220 ) ) ;
#79822=CARTESIAN_POINT ( 'NONE',  ( -115.6228709571501270, -24.15516710230297193, 10.28746687063727094 ) ) ;
#79823=FACE_OUTER_BOUND ( 'NONE', #36117, .T. ) ;
#79824=CARTESIAN_POINT ( 'NONE',  ( -29.62287095715004881, -23.39678932012542845, -1.443836140311830940 ) ) ;
#79828=FACE_OUTER_BOUND ( 'NONE', #52635, .T. ) ;
#79829=CARTESIAN_POINT ( 'NONE',  ( -3.169371320753151977, 19.67850563098683736, -1.500000000000002220 ) ) ;
#79830=CARTESIAN_POINT ( 'NONE',  ( -75.49319773296825531, -24.83644354573578994, 8.397322867130100121 ) ) ;
#79831=CARTESIAN_POINT ( 'NONE',  ( 19.57267778704439820, -3.578973306870405047, -1.500000000000002220 ) ) ;
#79834=EDGE_CURVE ( 'NONE', #24959, #80860, #13824, .T. ) ;
#79836=DIRECTION ( 'NONE',  ( -3.773278334453079030E-23, 0.9999999999976377785, 2.173523156925979128E-06 ) ) ;
#79838=CARTESIAN_POINT ( 'NONE',  ( -6.767879454864726974, -19.68250801024624508, 11.49999999999999645 ) ) ;
#79840=EDGE_CURVE ( 'NONE', #45608, #75868, #15878, .T. ) ;
#79842=CARTESIAN_POINT ( 'NONE',  ( 19.47892149737544187, 11.75266795981601753, 11.49999999999999645 ) ) ;
#79844=VERTEX_POINT ( 'NONE', #53963 ) ;
#79845=B_SPLINE_SURFACE_WITH_KNOTS ( 'NONE', 3, 3, ( 
 ( #94070, #24556, #93063, #71247 ),
 ( #38785, #69746, #23544, #1736 ),
 ( #32675, #70242, #55532, #86462 ),
 ( #62641, #63651, #94574, #56033 ),
 ( #54521, #722, #86960, #85455 ),
 ( #15940, #17449, #40791, #48414 ),
 ( #77830, #8337, #39285, #79344 ) ),
 .UNSPECIFIED., .F., .F., .F.,
 ( 4, 3, 4 ),
 ( 4, 4 ),
 ( 0.0004766839783814058292, 0.1029713700210894145, 0.2054660560637974198 ),
 ( 0.6096490815589712398, 0.6109430970810473260 ),
 .UNSPECIFIED. ) ;
#79846=CARTESIAN_POINT ( 'NONE',  ( -62.62287095715006302, -24.50216790748098816, 0.6166512839513665911 ) ) ;
#79848=ORIENTED_EDGE ( 'NONE', *, *, #6099, .F. ) ;
#79849=CARTESIAN_POINT ( 'NONE',  ( 19.72175082351460063, -4.362005935662174316, 11.49999999999998934 ) ) ;
#79850=PLANE ( 'NONE',  #82523 ) ;
#79851=DIRECTION ( 'NONE',  ( -3.773278334453079030E-23, 0.9999999999976377785, 2.173523156925979128E-06 ) ) ;
#79854=ORIENTED_EDGE ( 'NONE', *, *, #30963, .T. ) ;
#79855=CARTESIAN_POINT ( 'NONE',  ( -0.1426030150137701236, -21.20389190742571373, -1.497999999999532594 ) ) ;
#79857=CARTESIAN_POINT ( 'NONE',  ( -14.99618758923778117, -13.25627519679515665, -1.500000000000002220 ) ) ;
#79858=VECTOR ( 'NONE', #83436, 1000.000000000000114 ) ;
#79859=CARTESIAN_POINT ( 'NONE',  ( 7.003190781191628744, -19.75400906848480176, 11.49999999999999645 ) ) ;
#79860=CARTESIAN_POINT ( 'NONE',  ( -29.68423682549979148, -25.16578243805031789, 6.412434776996143171 ) ) ;
#79862=CARTESIAN_POINT ( 'NONE',  ( 8.687672273659204691, 20.25853876245846408, -1.500000000000002220 ) ) ;
#79863=EDGE_CURVE ( 'NONE', #75137, #23622, #17552, .T. ) ;
#79864=CARTESIAN_POINT ( 'NONE',  ( -54.62287095715005592, -24.64965695001467694, 8.947790433994185832 ) ) ;
#79867=CARTESIAN_POINT ( 'NONE',  ( -49.50841769935764347, -25.18440252003702184, 3.984447925546727109 ) ) ;
#79868=CARTESIAN_POINT ( 'NONE',  ( -72.54528880141759828, -24.34968618360933590, 0.1864209137778795600 ) ) ;
#79869=EDGE_LOOP ( 'NONE', ( #67188, #30318, #47920, #74015 ) ) ;
#79870=DIRECTION ( 'NONE',  ( 0.000000000000000000, 2.173523156925980399E-06, -0.9999999999976378895 ) ) ;
#79871=VERTEX_POINT ( 'NONE', #31605 ) ;
#79873=DIRECTION ( 'NONE',  ( -3.773278334453079030E-23, 0.9999999999976377785, 2.173523156925979128E-06 ) ) ;
#79874=CARTESIAN_POINT ( 'NONE',  ( -101.2911250451791858, -25.27404695253231282, 3.130826079498485903 ) ) ;
#79875=CARTESIAN_POINT ( 'NONE',  ( -58.62287095715007013, -23.96127896941631619, -0.6493128931037843721 ) ) ;
#79876=CARTESIAN_POINT ( 'NONE',  ( -0.1859688948871585645, 20.53422428922035081, -1.500000000000002220 ) ) ;
#79877=VERTEX_POINT ( 'NONE', #23473 ) ;
#79881=CARTESIAN_POINT ( 'NONE',  ( -64.52287095715006160, -23.47593901973090169, -1.443836447538996870 ) ) ;
#79882=CARTESIAN_POINT ( 'NONE',  ( -22.28969446433750434, -1.297463027894488086, -1.500000000000002220 ) ) ;
#79886=ORIENTED_EDGE ( 'NONE', *, *, #74513, .F. ) ;
#79887=CARTESIAN_POINT ( 'NONE',  ( -42.62287095715003460, -24.33832256526968507, 0.1851278514119854834 ) ) ;
#79888=CARTESIAN_POINT ( 'NONE',  ( -63.62287095715003460, -23.48783264082478084, -1.443836473390069042 ) ) ;
#79890=CARTESIAN_POINT ( 'NONE',  ( 18.01467621842780176, -10.50282939286117667, 11.49999999999998934 ) ) ;
#79891=ORIENTED_EDGE ( 'NONE', *, *, #72579, .T. ) ;
#79892=CARTESIAN_POINT ( 'NONE',  ( -52.52287095715007581, -24.51283580621455727, 0.6167428607047122924 ) ) ;
#79893=VERTEX_POINT ( 'NONE', #8275 ) ;
#79896=CARTESIAN_POINT ( 'NONE',  ( -69.33560399441930144, -25.25935264438429684, 7.166139204845690003 ) ) ;
#79897=CARTESIAN_POINT ( 'NONE',  ( 21.00884048613226440, 1.293913838035418040, -1.500000000000002220 ) ) ;
#79898=EDGE_LOOP ( 'NONE', ( #99607, #49347, #51105, #90482 ) ) ;
#79899=CARTESIAN_POINT ( 'NONE',  ( -69.52287095715006160, -23.48786465467241058, 11.44779295918254647 ) ) ;
#79901=CARTESIAN_POINT ( 'NONE',  ( -120.6237998820897843, -24.92592662359561118, 8.075495903017998245 ) ) ;
#79902=B_SPLINE_CURVE_WITH_KNOTS ( 'NONE', 3,
 ( #30744, #77900, #77402, #54591, #37371, #22118 ),
 .UNSPECIFIED., .F., .F.,
 ( 4, 2, 4 ),
 ( 6.391158118973930141E-06, 0.001387004593080795036, 0.002767618028042615873 ),
 .UNSPECIFIED. ) ;
#79904=CARTESIAN_POINT ( 'NONE',  ( -101.1119640259560271, -25.03152421035094832, 7.433728220542129783 ) ) ;
#79906=CARTESIAN_POINT ( 'NONE',  ( -59.56671735520578892, -23.48783264082476308, -1.443836473390097908 ) ) ;
#79907=CARTESIAN_POINT ( 'NONE',  ( -21.63489631200954122, -1.325961216813365429, -1.500000000000002220 ) ) ;
#79909=ADVANCED_FACE ( 'NONE', ( #14876 ), #70173, .T. ) ;
#79910=CARTESIAN_POINT ( 'NONE',  ( -2.380169663812839342, 22.11153957539610104, 11.49999999999999645 ) ) ;
#79914=VERTEX_POINT ( 'NONE', #1673 ) ;
#79915=CARTESIAN_POINT ( 'NONE',  ( -118.6228709571500559, -24.64965695001469115, 8.947790433994175174 ) ) ;
#79916=ORIENTED_EDGE ( 'NONE', *, *, #83583, .F. ) ;
#79917=VERTEX_POINT ( 'NONE', #41746 ) ;
#79920=CARTESIAN_POINT ( 'NONE',  ( 1.109688723463823301, -20.12803150795971874, -1.500000000000002220 ) ) ;
#79921=EDGE_CURVE ( 'NONE', #47216, #20204, #68307, .T. ) ;
#79924=CARTESIAN_POINT ( 'NONE',  ( -130.5728709571500303, -24.13533882933943175, 10.52299274931600337 ) ) ;
#79925=CARTESIAN_POINT ( 'NONE',  ( -9.774569144048079750, -20.17623354167628946, -1.500000000000002220 ) ) ;
#79927=ORIENTED_EDGE ( 'NONE', *, *, #40955, .T. ) ;
#79932=FACE_OUTER_BOUND ( 'NONE', #22387, .T. ) ;
#79934=EDGE_CURVE ( 'NONE', #89410, #63331, #64599, .T. ) ;
#79935=CARTESIAN_POINT ( 'NONE',  ( -97.23961491194229723, -25.30559561715418226, 6.147794833475641596 ) ) ;
#79936=CARTESIAN_POINT ( 'NONE',  ( -10.82925958622295859, 16.30987832687952022, -1.500000000000002220 ) ) ;
#79937=B_SPLINE_CURVE_WITH_KNOTS ( 'NONE', 3,
 ( #41138, #88809, #49758, #71586, #34518, #87804 ),
 .UNSPECIFIED., .F., .F.,
 ( 4, 2, 4 ),
 ( 0.000000000000000000, 0.0002343639316654294483, 0.0004687278633308588965 ),
 .UNSPECIFIED. ) ;
#79939=CARTESIAN_POINT ( 'NONE',  ( -57.62287095715004881, -29.50248528299804818, 1.056150453629034924 ) ) ;
#79941=CARTESIAN_POINT ( 'NONE',  ( -20.54356019850136050, 6.435454313062578535, -1.500000000000002220 ) ) ;
#79943=B_SPLINE_CURVE_WITH_KNOTS ( 'NONE', 3,
 ( #90879, #74651, #81273, #13244, #73664, #4658 ),
 .UNSPECIFIED., .F., .F.,
 ( 4, 2, 4 ),
 ( 0.000000000000000000, 0.001380901958385391580, 0.002761803916770783161 ),
 .UNSPECIFIED. ) ;
#79944=CARTESIAN_POINT ( 'NONE',  ( -114.5228709571500758, -23.47593901973090524, -1.443836447538996204 ) ) ;
#79945=CARTESIAN_POINT ( 'NONE',  ( -123.5228709571500190, -23.73934037231757443, 11.05740245334327732 ) ) ;
#79946=DIRECTION ( 'NONE',  ( -3.773278334444167608E-23, 1.000000000000000000, 0.000000000000000000 ) ) ;
#79947=B_SPLINE_CURVE_WITH_KNOTS ( 'NONE', 3,
 ( #40536, #94804, #31914, #79582 ),
 .UNSPECIFIED., .F., .F.,
 ( 4, 4 ),
 ( 2.775557561562891351E-17, 0.0001000000000000167286 ),
 .UNSPECIFIED. ) ;
#79948=CARTESIAN_POINT ( 'NONE',  ( -19.87571804785047647, -11.42512898079034400, -1.500000000000002220 ) ) ;
#79951=CARTESIAN_POINT ( 'NONE',  ( -53.54760685552204080, -24.15543982623906771, -0.2315651400026670914 ) ) ;
#79952=CARTESIAN_POINT ( 'NONE',  ( 8.649182803842551337, -18.14983140373652404, 11.49999999999999645 ) ) ;
#79953=CARTESIAN_POINT ( 'NONE',  ( -40.55620429048338593, -25.00182538069145011, 7.747789668545099317 ) ) ;
#79954=CARTESIAN_POINT ( 'NONE',  ( -31.52287095715007581, -23.96127896942127933, -0.6493128930940336163 ) ) ;
#79956=CARTESIAN_POINT ( 'NONE',  ( -102.6228709571500559, -24.64898659630368272, 1.056161002820829697 ) ) ;
#79957=CARTESIAN_POINT ( 'NONE',  ( -82.52287095715006160, -23.47596703998600631, 11.44779298504228571 ) ) ;
#79958=CARTESIAN_POINT ( 'NONE',  ( 17.59243620335545799, -9.192777620008959261, 11.49999999999998934 ) ) ;
#79960=CARTESIAN_POINT ( 'NONE',  ( -16.89733858281218204, -10.06102416988892934, -1.500000000000002220 ) ) ;
#79961=CARTESIAN_POINT ( 'NONE',  ( -42.54640892709206668, -24.15543982623907127, -0.2315651400026575435 ) ) ;
#79966=CARTESIAN_POINT ( 'NONE',  ( -39.11375990658831370, -25.30200599664514982, 4.685637363869906480 ) ) ;
#79967=CARTESIAN_POINT ( 'NONE',  ( 20.62939718826500979, -0.8834638802319035866, 11.49999999999999645 ) ) ;
#79970=VECTOR ( 'NONE', #52605, 1000.000000000000114 ) ;
#79971=CARTESIAN_POINT ( 'NONE',  ( 2.010693963185784749, 22.50221635003889276, 11.49999999999999645 ) ) ;
#79972=EDGE_CURVE ( 'NONE', #80402, #5790, #86895, .T. ) ;
#79974=CARTESIAN_POINT ( 'NONE',  ( -69.56233234027952506, -25.25639530571745439, 6.775360290800271912 ) ) ;
#79976=CARTESIAN_POINT ( 'NONE',  ( -72.62287095715004170, -24.50321055353805377, 9.387540953477529371 ) ) ;
#79978=CARTESIAN_POINT ( 'NONE',  ( -110.5228709571500474, -24.15431212366389957, -0.2830839119429225947 ) ) ;
#79979=CARTESIAN_POINT ( 'NONE',  ( -41.26959558397305727, -29.50249893827660941, 7.338705366995167623 ) ) ;
#79981=CARTESIAN_POINT ( 'NONE',  ( -79.89247415061277025, -25.31596245313187055, 5.073623374384617968 ) ) ;
#79982=CARTESIAN_POINT ( 'NONE',  ( -21.19308438721250099, -8.479022899233653376, -1.500000000000002220 ) ) ;
#79983=DIRECTION ( 'NONE',  ( 1.000000000000000000, 3.773278334444167608E-23, 8.201307833595939069E-29 ) ) ;
#79984=DIRECTION ( 'NONE',  ( -3.773278334453079618E-23, 0.9999999999976377785, 2.173523156925979975E-06 ) ) ;
#79985=CARTESIAN_POINT ( 'NONE',  ( -63.50463970142624959, -24.15620529776628089, 10.23563542870660470 ) ) ;
#79986=B_SPLINE_CURVE_WITH_KNOTS ( 'NONE', 3,
 ( #24152, #32768, #33265, #62744 ),
 .UNSPECIFIED., .F., .F.,
 ( 4, 4 ),
 ( 0.000000000000000000, 1.000000000000000000 ),
 .UNSPECIFIED. ) ;
#79987=CARTESIAN_POINT ( 'NONE',  ( -21.66288588771858770, -5.991481186202806342, 11.49999999999999645 ) ) ;
#79988=ORIENTED_EDGE ( 'NONE', *, *, #70685, .T. ) ;
#79989=CARTESIAN_POINT ( 'NONE',  ( -43.52946602040498902, -24.65952944569304606, 1.056160979905694131 ) ) ;
#79990=CARTESIAN_POINT ( 'NONE',  ( 7.969717912702302343, -20.46423023992739942, -1.500000000000002220 ) ) ;
#79991=CARTESIAN_POINT ( 'NONE',  ( -54.62287095715007013, -23.96127896941632685, -0.6493128931037892571 ) ) ;
#79992=ADVANCED_FACE ( 'NONE', ( #78267 ), #40231, .T. ) ;
#79996=CARTESIAN_POINT ( 'NONE',  ( -92.52287095715006160, -24.64898659630529210, 1.056161002820827921 ) ) ;
#79998=VERTEX_POINT ( 'NONE', #32611 ) ;
#79999=CARTESIAN_POINT ( 'NONE',  ( -54.54194454780496670, -24.35071581493543391, 9.817618358456034144 ) ) ;
#80000=CARTESIAN_POINT ( 'NONE',  ( 3.385237411341575964, -20.22741857368478335, -1.500000000000002220 ) ) ;
#80001=ORIENTED_EDGE ( 'NONE', *, *, #81643, .T. ) ;
#80002=ORIENTED_EDGE ( 'NONE', *, *, #98334, .F. ) ;
#80004=ORIENTED_EDGE ( 'NONE', *, *, #54162, .F. ) ;
#80005=CARTESIAN_POINT ( 'NONE',  ( -84.62287095715004170, -24.65952944569304606, 1.056160979905699460 ) ) ;
#80006=CARTESIAN_POINT ( 'NONE',  ( 14.65057173600216345, 17.85730367728733725, -1.500000000000002220 ) ) ;
#80007=CARTESIAN_POINT ( 'NONE',  ( -104.5872714728782711, -24.51419770103158768, 9.386484678747164523 ) ) ;
#80008=CARTESIAN_POINT ( 'NONE',  ( -20.32544160278596834, -1.370942541838689799, -1.500000000000002220 ) ) ;
#80010=ORIENTED_EDGE ( 'NONE', *, *, #18417, .T. ) ;
#80011=CARTESIAN_POINT ( 'NONE',  ( -71.70008735307283132, -25.22833616190947126, 6.373748403976279064 ) ) ;
#80012=EDGE_CURVE ( 'NONE', #86729, #50770, #63477, .T. ) ;
#80013=CARTESIAN_POINT ( 'NONE',  ( -88.62287095715004170, -24.34917612406838217, 0.1852690917426653427 ) ) ;
#80014=ADVANCED_FACE ( 'NONE', ( #8778 ), #10277, .T. ) ;
#80015=PLANE ( 'NONE',  #28676 ) ;
#80018=CARTESIAN_POINT ( 'NONE',  ( -101.6228709571500559, -29.50247984919015209, -1.443849546365050029 ) ) ;
#80019=CARTESIAN_POINT ( 'NONE',  ( -49.10641598061040725, -25.31573638291652273, 4.048599298564869109 ) ) ;
#80021=ADVANCED_FACE ( 'NONE', ( #41234 ), #9266, .F. ) ;
#80023=CARTESIAN_POINT ( 'NONE',  ( -12.88759680649768136, 16.30154091734715749, -1.500000000000002220 ) ) ;
#80025=DIRECTION ( 'NONE',  ( -1.000000000000000000, -3.773278334444166432E-23, -8.201307841325785021E-29 ) ) ;
#80027=B_SPLINE_CURVE_WITH_KNOTS ( 'NONE', 3,
 ( #87018, #81413, #34244, #48474 ),
 .UNSPECIFIED., .F., .F.,
 ( 4, 4 ),
 ( 0.000000000000000000, 9.999999999998897304E-05 ),
 .UNSPECIFIED. ) ;
#80028=DIRECTION ( 'NONE',  ( 0.000000000000000000, 2.173523156925980399E-06, -0.9999999999976378895 ) ) ;
#80029=CARTESIAN_POINT ( 'NONE',  ( -97.52287095715009002, -23.96177878511308990, 10.65340807706329329 ) ) ;
#80031=ORIENTED_EDGE ( 'NONE', *, *, #36786, .F. ) ;
#80032=B_SPLINE_CURVE_WITH_KNOTS ( 'NONE', 3,
 ( #50520, #56149, #50037, #95696, #79466, #34801, #96203, #80970 ),
 .UNSPECIFIED., .F., .F.,
 ( 4, 2, 2, 4 ),
 ( 0.000000000000000000, 0.002001098010032798143, 0.003001647015049197214, 0.004002196020065596285 ),
 .UNSPECIFIED. ) ;
#80034=DIRECTION ( 'NONE',  ( -3.773278334444166432E-23, 1.000000000000000000, 0.000000000000000000 ) ) ;
#80035=CARTESIAN_POINT ( 'NONE',  ( -78.52287095715006160, -23.47593901973090169, -1.443836447538996648 ) ) ;
#80037=CARTESIAN_POINT ( 'NONE',  ( -19.11006845027251799, 11.06304553819242642, 11.49999999999999645 ) ) ;
#80038=ORIENTED_EDGE ( 'NONE', *, *, #76059, .T. ) ;
#80039=CARTESIAN_POINT ( 'NONE',  ( -49.16102892102028932, -25.15009172915296887, 7.003546792922761277 ) ) ;
#80040=CARTESIAN_POINT ( 'NONE',  ( -22.11960324842224423, 4.537628740662121629, -1.500000000000002220 ) ) ;
#80041=DIRECTION ( 'NONE',  ( 0.000000000000000000, 0.9999999999976377785, 2.173523156925979975E-06 ) ) ;
#80042=ORIENTED_EDGE ( 'NONE', *, *, #53796, .T. ) ;
#80043=ORIENTED_EDGE ( 'NONE', *, *, #95707, .F. ) ;
#80045=EDGE_CURVE ( 'NONE', #72031, #17423, #79780, .T. ) ;
#80049=CARTESIAN_POINT ( 'NONE',  ( -14.54676392617323266, -15.37779485849079464, -1.500000000000002220 ) ) ;
#80054=CARTESIAN_POINT ( 'NONE',  ( -2.380169663812839342, 22.11153957539610104, -1.500000000000002220 ) ) ;
#80055=CARTESIAN_POINT ( 'NONE',  ( -114.5554611002867773, -23.96119346886881374, -0.6495511937831859317 ) ) ;
#80057=ORIENTED_EDGE ( 'NONE', *, *, #50244, .T. ) ;
#80059=CARTESIAN_POINT ( 'NONE',  ( -37.48487686491367299, -24.51314013834316796, 0.6176544820404176184 ) ) ;
#80060=CARTESIAN_POINT ( 'NONE',  ( -5.977879402576776968, -18.46583800616800630, 11.49999999999999645 ) ) ;
#80061=EDGE_CURVE ( 'NONE', #90955, #4409, #49863, .T. ) ;
#80062=CARTESIAN_POINT ( 'NONE',  ( -41.68476140872422775, -25.21340872514199916, 3.506346521580342213 ) ) ;
#80064=B_SPLINE_CURVE_WITH_KNOTS ( 'NONE', 3,
 ( #91295, #21764, #52738, #60862, #83677, #14159 ),
 .UNSPECIFIED., .F., .F.,
 ( 4, 2, 4 ),
 ( 1.570887131794952276E-05, 0.001396322306279765193, 0.002776935741241580609 ),
 .UNSPECIFIED. ) ;
#80066=CARTESIAN_POINT ( 'NONE',  ( -18.70048401425367501, 5.426029767813830063, -1.500000000000002220 ) ) ;
#80067=CARTESIAN_POINT ( 'NONE',  ( -9.048234560742015375, 19.43086790383670603, 11.49999999999998934 ) ) ;
#80068=CARTESIAN_POINT ( 'NONE',  ( -56.62287095715005592, -23.48786465467241413, 11.44779295918254824 ) ) ;
#80069=CARTESIAN_POINT ( 'NONE',  ( -26.98755670591954114, -24.57999526489839326, 1.764415294430758507 ) ) ;
#80070=FACE_OUTER_BOUND ( 'NONE', #29191, .T. ) ;
#80071=CARTESIAN_POINT ( 'NONE',  ( -123.6228709571500559, -23.47596703998600631, 11.44779298504227860 ) ) ;
#80072=CARTESIAN_POINT ( 'NONE',  ( -22.72798930328562150, -0.2126449523330483371, -1.500000000000002220 ) ) ;
#80073=EDGE_CURVE ( 'NONE', #26998, #15184, #40456, .T. ) ;
#80075=CARTESIAN_POINT ( 'NONE',  ( -54.52287095715006870, -29.50250243563736774, 8.947779886222146928 ) ) ;
#80077=CARTESIAN_POINT ( 'NONE',  ( 11.38277053702107899, 16.36964821499295653, 11.49999999999999645 ) ) ;
#80078=CARTESIAN_POINT ( 'NONE',  ( -104.5531608873337035, -24.15543982623907482, -0.2315651400026580709 ) ) ;
#80079=CARTESIAN_POINT ( 'NONE',  ( -39.55295621575191234, -23.96169478059712787, 10.65365249895718769 ) ) ;
#80080=CARTESIAN_POINT ( 'NONE',  ( -31.52287095715006160, -29.50248528299804818, 1.056150453629029817 ) ) ;
#80083=CARTESIAN_POINT ( 'NONE',  ( -32.99705628988545669, -25.31516574674648368, 3.894478520810415567 ) ) ;
#80085=CARTESIAN_POINT ( 'NONE',  ( -18.45943378446990835, 11.37049804852326140, 11.49999999999998934 ) ) ;
#80086=DIRECTION ( 'NONE',  ( 3.773278334444167608E-23, -1.000000000000000000, 0.000000000000000000 ) ) ;
#80087=CARTESIAN_POINT ( 'NONE',  ( -19.44331071757236273, 1.017868325215548708, -1.500000000000002220 ) ) ;
#80088=CARTESIAN_POINT ( 'NONE',  ( -125.5228709571500616, -29.50249982740957577, 7.747779886224967605 ) ) ;
#80091=DIRECTION ( 'NONE',  ( -3.773278334444167608E-23, 1.000000000000000000, 0.000000000000000000 ) ) ;
#80092=CARTESIAN_POINT ( 'NONE',  ( 20.35601985306173134, -1.938729116259007679, 11.49999999999999645 ) ) ;
#80093=CARTESIAN_POINT ( 'NONE',  ( -110.6228709571500701, -23.48783264082479505, -1.443836473390060160 ) ) ;
#80094=CARTESIAN_POINT ( 'NONE',  ( -118.6228709571500701, -23.96127896941633040, -0.6493128931037773777 ) ) ;
#80096=FACE_OUTER_BOUND ( 'NONE', #81292, .T. ) ;
#80099=CARTESIAN_POINT ( 'NONE',  ( -49.27764846858840997, -25.26180677598144086, 6.145204968850301874 ) ) ;
#80100=CARTESIAN_POINT ( 'NONE',  ( -129.5895376238166818, -23.48783264082478794, -1.443836473390056607 ) ) ;
#80101=B_SPLINE_CURVE_WITH_KNOTS ( 'NONE', 3,
 ( #9740, #39181, #93967, #10238 ),
 .UNSPECIFIED., .F., .F.,
 ( 4, 4 ),
 ( 0.000000000000000000, 9.999999999998897304E-05 ),
 .UNSPECIFIED. ) ;
#80102=DIRECTION ( 'NONE',  ( -3.773278334453079618E-23, 0.9999999999976377785, 2.173523156925979975E-06 ) ) ;
#80103=VERTEX_POINT ( 'NONE', #27005 ) ;
#80104=CARTESIAN_POINT ( 'NONE',  ( -66.64658286559381395, -23.73791477778911840, 11.05961554403170766 ) ) ;
#80105=CARTESIAN_POINT ( 'NONE',  ( -12.88233675513024856, -19.01995677650982230, 11.49999999999999645 ) ) ;
#80106=CARTESIAN_POINT ( 'NONE',  ( 12.47407908559008760, -19.03963781694049473, -1.500000000000002220 ) ) ;
#80107=CARTESIAN_POINT ( 'NONE',  ( -110.5871102190748729, -24.83644354573579349, 8.397322867130096569 ) ) ;
#80108=CARTESIAN_POINT ( 'NONE',  ( -98.52287095715006160, -23.48783264082477018, -1.443836473390087916 ) ) ;
#80109=CARTESIAN_POINT ( 'NONE',  ( -90.49972952456502640, -24.92564183028978775, 1.928384488918253092 ) ) ;
#80110=CARTESIAN_POINT ( 'NONE',  ( -70.52287095715009002, -23.85196035786899671, -0.8779234886475163480 ) ) ;
#80111=CARTESIAN_POINT ( 'NONE',  ( -82.58953762381672448, -23.48783264082478084, -1.443836473390065933 ) ) ;
#80112=CARTESIAN_POINT ( 'NONE',  ( 3.414333255021221092, 21.62243999391013105, -1.500000000000002220 ) ) ;
#80115=CARTESIAN_POINT ( 'NONE',  ( -115.6228709571500701, -24.15431212366392089, -0.2830839119429090500 ) ) ;
#80116=CARTESIAN_POINT ( 'NONE',  ( -71.33443329732202187, -25.30573833935151740, 5.086063791536371781 ) ) ;
#80117=CARTESIAN_POINT ( 'NONE',  ( -98.99594346619821295, -25.31200630955432018, 5.589963903709685766 ) ) ;
#80120=CARTESIAN_POINT ( 'NONE',  ( -19.81292649638395531, 4.959676026661640869, -1.500000000000002220 ) ) ;
#80121=ORIENTED_EDGE ( 'NONE', *, *, #78480, .F. ) ;
#80122=B_SPLINE_CURVE_WITH_KNOTS ( 'NONE', 3,
 ( #16207, #68999, #39552, #60903 ),
 .UNSPECIFIED., .F., .F.,
 ( 4, 4 ),
 ( 0.000000000000000000, 1.000000000000000000 ),
 .UNSPECIFIED. ) ;
#80123=ORIENTED_EDGE ( 'NONE', *, *, #55861, .F. ) ;
#80124=CARTESIAN_POINT ( 'NONE',  ( -11.53412672884717871, -19.92380006517282709, -1.500000000000002220 ) ) ;
#80125=FACE_OUTER_BOUND ( 'NONE', #92016, .T. ) ;
#80126=ADVANCED_FACE ( 'NONE', ( #5162 ), #44234, .F. ) ;
#80127=ORIENTED_EDGE ( 'NONE', *, *, #2367, .F. ) ;
#80128=CARTESIAN_POINT ( 'NONE',  ( -101.5562042904833930, -24.65952944569304606, 1.056160979905701236 ) ) ;
#80129=ADVANCED_FACE ( 'NONE', ( #73187 ), #24025, .T. ) ;
#80131=EDGE_CURVE ( 'NONE', #68269, #49130, #24732, .T. ) ;
#80134=CARTESIAN_POINT ( 'NONE',  ( -21.04715019690976874, -3.721878931196799467, 11.49999999999999645 ) ) ;
#80135=ORIENTED_EDGE ( 'NONE', *, *, #75428, .F. ) ;
#80138=CARTESIAN_POINT ( 'NONE',  ( 2.725811458822067657, 22.07344620009914138, -1.500000000000002220 ) ) ;
#80139=CARTESIAN_POINT ( 'NONE',  ( 9.361532043782798240, 18.45020211870636118, -1.500000000000002220 ) ) ;
#80141=B_SPLINE_CURVE_WITH_KNOTS ( 'NONE', 3,
 ( #25621, #25108, #55586, #62701, #93617, #71303, #46965, #87527 ),
 .UNSPECIFIED., .F., .F.,
 ( 4, 2, 2, 4 ),
 ( 0.000000000000000000, 0.002001098010032802479, 0.003001647015049203719, 0.004002196020065604959 ),
 .UNSPECIFIED. ) ;
#80142=ORIENTED_EDGE ( 'NONE', *, *, #12281, .T. ) ;
#80144=CARTESIAN_POINT ( 'NONE',  ( -110.6228709571500559, -24.99156045073393173, 7.747789690856161648 ) ) ;
#80146=CARTESIAN_POINT ( 'NONE',  ( -83.62287095715005592, -24.50321055353805377, 9.387540953477522265 ) ) ;
#80148=FACE_OUTER_BOUND ( 'NONE', #77002, .T. ) ;
#80150=CARTESIAN_POINT ( 'NONE',  ( 0.8369575198195864374, -20.89415947959451003, -1.500000000000002220 ) ) ;
#80151=EDGE_CURVE ( 'NONE', #58306, #5356, #468, .T. ) ;
#80152=CARTESIAN_POINT ( 'NONE',  ( -15.17958814119055155, -15.74432251006154715, 11.49999999999999645 ) ) ;
#80154=CARTESIAN_POINT ( 'NONE',  ( -107.6228709571500417, -23.73934037231757799, 11.05740245334328264 ) ) ;
#80156=CARTESIAN_POINT ( 'NONE',  ( 22.48772827135616126, 0.8316936486096353498, 11.49999999999998934 ) ) ;
#80157=CARTESIAN_POINT ( 'NONE',  ( -17.10473743203234775, -12.04273770408705246, -1.500000000000002220 ) ) ;
#80158=DIRECTION ( 'NONE',  ( -3.773278334444166432E-23, 1.000000000000000000, 0.000000000000000000 ) ) ;
#80161=EDGE_CURVE ( 'NONE', #83380, #89496, #93744, .T. ) ;
#80162=ORIENTED_EDGE ( 'NONE', *, *, #78721, .T. ) ;
#80163=ORIENTED_EDGE ( 'NONE', *, *, #96389, .T. ) ;
#80165=CARTESIAN_POINT ( 'NONE',  ( -52.49586652078557591, -24.34968618360933945, 0.1864209137778880532 ) ) ;
#80167=EDGE_CURVE ( 'NONE', #85963, #98513, #84037, .T. ) ;
#80168=CARTESIAN_POINT ( 'NONE',  ( -2.751442626040462081, 21.25944542233241563, -1.500000000000002220 ) ) ;
#80170=CARTESIAN_POINT ( 'NONE',  ( -95.55620429048337883, -23.47593901973091235, -1.443836447539001089 ) ) ;
#80171=CARTESIAN_POINT ( 'NONE',  ( -17.90976863334866920, 11.11529090135583075, -1.500000000000002220 ) ) ;
#80172=CARTESIAN_POINT ( 'NONE',  ( -30.45987962603713939, -25.30658194294376173, 6.147639284700202822 ) ) ;
#80175=DIRECTION ( 'NONE',  ( -1.000000000000000000, -3.773278334444166432E-23, -8.201307841325785021E-29 ) ) ;
#80176=CARTESIAN_POINT ( 'NONE',  ( 18.22792733936863030, -12.41963300964812156, -1.500000000000002220 ) ) ;
#80177=ORIENTED_EDGE ( 'NONE', *, *, #6982, .T. ) ;
#80178=LINE ( 'NONE', #2071, #64872 ) ;
#80180=CARTESIAN_POINT ( 'NONE',  ( -111.6228709571501128, -24.35013146730204525, 9.818937971375108376 ) ) ;
#80181=CARTESIAN_POINT ( 'NONE',  ( -41.14436886340001820, -25.31624709515424598, 5.395510681755817828 ) ) ;
#80182=EDGE_CURVE ( 'NONE', #39193, #81122, #61955, .T. ) ;
#80183=CARTESIAN_POINT ( 'NONE',  ( -62.64802848561124193, -23.73791477778912196, 11.05961554403171121 ) ) ;
#80184=CARTESIAN_POINT ( 'NONE',  ( -26.29960327999231495, -24.65857663733338967, 2.249178454020304585 ) ) ;
#80187=CARTESIAN_POINT ( 'NONE',  ( -14.61619677566029729, 15.53698580111986693, -1.500000000000002220 ) ) ;
#80188=CARTESIAN_POINT ( 'NONE',  ( -91.62287095715004170, -23.47596703998600631, 11.44779298504227860 ) ) ;
#80189=CARTESIAN_POINT ( 'NONE',  ( -124.5228709571500616, -23.72747288104470798, -1.053458166803225460 ) ) ;
#80191=DIRECTION ( 'NONE',  ( 0.000000000000000000, -0.9999999999976377785, -2.173523156925979128E-06 ) ) ;
#80192=PLANE ( 'NONE',  #68607 ) ;
#80193=CARTESIAN_POINT ( 'NONE',  ( -14.16962031475959272, 17.58799634409329471, -1.500000000000002220 ) ) ;
#80198=CARTESIAN_POINT ( 'NONE',  ( -19.50520112914412252, -2.896358124273927359, 11.49999999999999645 ) ) ;
#80199=FACE_OUTER_BOUND ( 'NONE', #90921, .T. ) ;
#80200=CARTESIAN_POINT ( 'NONE',  ( -96.62287095715005592, -23.47593901973091235, -1.443836447539001089 ) ) ;
#80202=ORIENTED_EDGE ( 'NONE', *, *, #68508, .T. ) ;
#80203=DIRECTION ( 'NONE',  ( 0.000000000000000000, -2.173523156925980399E-06, 0.9999999999976378895 ) ) ;
#80205=CARTESIAN_POINT ( 'NONE',  ( -105.5228709571501042, -24.92604778743017135, 8.074972756849355449 ) ) ;
#80206=PLANE ( 'NONE',  #42122 ) ;
#80207=CARTESIAN_POINT ( 'NONE',  ( -68.62287095715005592, -24.65952944569304606, 1.056160979905698794 ) ) ;
#80209=CARTESIAN_POINT ( 'NONE',  ( -81.87216895719394927, -25.23777318042872508, 6.379003627969344947 ) ) ;
#80210=CARTESIAN_POINT ( 'NONE',  ( -11.78406182805296254, 15.88391379356440503, 11.49999999999998934 ) ) ;
#80212=CARTESIAN_POINT ( 'NONE',  ( 8.147030896810244727, 18.52525024547675869, 11.49999999999999645 ) ) ;
#80216=CARTESIAN_POINT ( 'NONE',  ( -65.52287095715006160, -23.47596703998600631, 11.44779298504228748 ) ) ;
#80219=CARTESIAN_POINT ( 'NONE',  ( -82.62287095715005592, -23.47593901973091235, -1.443836447539004642 ) ) ;
#80222=CARTESIAN_POINT ( 'NONE',  ( 19.28819943863484454, -5.468471092112969778, 11.49999999999998934 ) ) ;
#80227=CARTESIAN_POINT ( 'NONE',  ( -32.62287095715005592, -24.66019654487199020, 8.947790411086137041 ) ) ;
#80228=CARTESIAN_POINT ( 'NONE',  ( -89.62287095715004170, -29.50248528299804818, 1.056150453629040253 ) ) ;
#80229=CARTESIAN_POINT ( 'NONE',  ( -79.39460018469020497, -25.28987694977702816, 5.623653258205846939 ) ) ;
#80231=B_SPLINE_CURVE_WITH_KNOTS ( 'NONE', 3,
 ( #86521, #93622, #95141, #9395, #2807, #32734 ),
 .UNSPECIFIED., .F., .F.,
 ( 4, 2, 4 ),
 ( 6.384118678608569234E-06, 0.001386860460828372166, 0.002767336802978135821 ),
 .UNSPECIFIED. ) ;
#80232=CARTESIAN_POINT ( 'NONE',  ( -73.62685968689160632, -24.51314013834315375, 0.6176544820404104019 ) ) ;
#80234=ADVANCED_FACE ( 'NONE', ( #2561 ), #86280, .F. ) ;
#80235=CARTESIAN_POINT ( 'NONE',  ( -99.90567954317651811, -25.30060005375480969, 6.009289253917325269 ) ) ;
#80236=VERTEX_POINT ( 'NONE', #56360 ) ;
#80237=EDGE_CURVE ( 'NONE', #94885, #27247, #78147, .T. ) ;
#80238=CARTESIAN_POINT ( 'NONE',  ( -15.70679263237263434, -12.88635299011707502, 11.49999999999998934 ) ) ;
#80240=CARTESIAN_POINT ( 'NONE',  ( -32.49651614175236602, -24.15543982623907127, -0.2315651400026567941 ) ) ;
#80242=CARTESIAN_POINT ( 'NONE',  ( -127.5903467349210132, -23.73791477778912551, 11.05961554403169345 ) ) ;
#80244=CARTESIAN_POINT ( 'NONE',  ( -59.56672357952546548, -23.48786465467241058, 11.44779295918255357 ) ) ;
#80247=CARTESIAN_POINT ( 'NONE',  ( -86.62287095715004170, -23.47593901973091235, -1.443836447539002865 ) ) ;
#80248=CARTESIAN_POINT ( 'NONE',  ( 19.38521227897113874, -8.589346653930519437, 11.49999999999999645 ) ) ;
#80250=B_SPLINE_CURVE_WITH_KNOTS ( 'NONE', 3,
 ( #41719, #80262, #65568, #72659, #81760, #3156 ),
 .UNSPECIFIED., .F., .F.,
 ( 4, 2, 4 ),
 ( 0.000000000000000000, 0.001380901958385390930, 0.002761803916770781860 ),
 .UNSPECIFIED. ) ;
#80251=CARTESIAN_POINT ( 'NONE',  ( 17.13038851031509680, -14.05419017248541813, -1.500000000000002220 ) ) ;
#80253=CARTESIAN_POINT ( 'NONE',  ( -16.28974412851428255, -12.55652860423730388, -1.500000000000002220 ) ) ;
#80255=CARTESIAN_POINT ( 'NONE',  ( -111.6228709571500559, -23.48783264082479505, -1.443836473390060604 ) ) ;
#80257=CARTESIAN_POINT ( 'NONE',  ( -37.22287095715005734, -23.47596703998600276, 11.44779298504227683 ) ) ;
#80259=ORIENTED_EDGE ( 'NONE', *, *, #82231, .F. ) ;
#80260=ORIENTED_EDGE ( 'NONE', *, *, #80182, .F. ) ;
#80262=CARTESIAN_POINT ( 'NONE',  ( -116.6228709571500417, -23.72773821059535848, 11.05748984161097503 ) ) ;
#80265=CARTESIAN_POINT ( 'NONE',  ( 11.71144010791963730, -17.07555522294065753, -1.500000000000002220 ) ) ;
#80266=CARTESIAN_POINT ( 'NONE',  ( -20.76051858633888259, -6.224802954461835292, 11.49999999999999645 ) ) ;
#80270=CARTESIAN_POINT ( 'NONE',  ( -9.774569144048079750, -20.17623354167628946, -1.500000000000002220 ) ) ;
#80272=CARTESIAN_POINT ( 'NONE',  ( -71.62287095715005592, -23.73907113216990794, -1.053371485793230811 ) ) ;
#80274=CARTESIAN_POINT ( 'NONE',  ( -45.58953762381671737, -24.99132157543083821, 2.256160258750496084 ) ) ;
#80275=CARTESIAN_POINT ( 'NONE',  ( -98.62287095715005592, -29.50248528299804818, 1.056150453629042030 ) ) ;
#80277=ORIENTED_EDGE ( 'NONE', *, *, #92775, .F. ) ;
#80279=CARTESIAN_POINT ( 'NONE',  ( -46.54046596679725667, -24.35071581493542325, 9.817618358456032368 ) ) ;
#80280=ORIENTED_EDGE ( 'NONE', *, *, #3420, .T. ) ;
#80281=VECTOR ( 'NONE', #54053, 1000.000000000000114 ) ;
#80282=DIRECTION ( 'NONE',  ( 3.773278334444167608E-23, -1.000000000000000000, 0.000000000000000000 ) ) ;
#80283=CARTESIAN_POINT ( 'NONE',  ( -0.06837171988653999166, -21.26218376953697486, -1.500000000000002220 ) ) ;
#80284=ORIENTED_EDGE ( 'NONE', *, *, #39530, .F. ) ;
#80285=CARTESIAN_POINT ( 'NONE',  ( -100.5101194842158634, -25.12316535023712660, 7.100618891458206683 ) ) ;
#80286=CARTESIAN_POINT ( 'NONE',  ( 3.468383421097696928, -21.53508805063734854, -1.500000000000002220 ) ) ;
#80287=FACE_OUTER_BOUND ( 'NONE', #11, .T. ) ;
#80290=CARTESIAN_POINT ( 'NONE',  ( -35.62287095715006302, -23.84047902841601285, -0.8780736468305813114 ) ) ;
#80291=CARTESIAN_POINT ( 'NONE',  ( 19.17057494584436839, 10.47865234463220396, -1.500000000000002220 ) ) ;
#80295=CARTESIAN_POINT ( 'NONE',  ( -85.58383951320973893, -24.83644354573578994, 8.397322867130101898 ) ) ;
#80296=AXIS2_PLACEMENT_3D ( 'NONE', #84888, #64089, #62569 ) ;
#80299=CARTESIAN_POINT ( 'NONE',  ( -99.62287095715005592, -23.47596703998600631, 11.44779298504227860 ) ) ;
#80302=CARTESIAN_POINT ( 'NONE',  ( -113.6228709571500275, -23.96127896941632685, -0.6493128931037774887 ) ) ;
#80303=CARTESIAN_POINT ( 'NONE',  ( -15.86343167427570577, 14.10970434637795634, -1.500000000000002220 ) ) ;
#80305=CARTESIAN_POINT ( 'NONE',  ( -30.56688274934923655, -25.56688301298833821, 3.825958421598584014 ) ) ;
#80306=EDGE_CURVE ( 'NONE', #47994, #47959, #51337, .T. ) ;
#80308=CARTESIAN_POINT ( 'NONE',  ( -118.6228709571500559, -29.50247984919015209, -1.443849546365046699 ) ) ;
#80309=CARTESIAN_POINT ( 'NONE',  ( 11.34002819025610087, 15.78594478779102950, 11.49999999999998934 ) ) ;
#80310=EDGE_CURVE ( 'NONE', #69320, #93091, #23439, .T. ) ;
#80311=CARTESIAN_POINT ( 'NONE',  ( -45.52502742233122746, -24.92564183028978775, 1.928384488918256645 ) ) ;
#80313=CARTESIAN_POINT ( 'NONE',  ( -2.678125609936932605, 19.29598960679622976, 11.49999999999999645 ) ) ;
#80315=CARTESIAN_POINT ( 'NONE',  ( -42.52287095715005449, -23.48786465467240347, 11.44779295918255180 ) ) ;
#80317=CARTESIAN_POINT ( 'NONE',  ( -97.52287095715009002, -24.51283580621364067, 0.6167428607019849185 ) ) ;
#80318=CARTESIAN_POINT ( 'NONE',  ( -89.50344290891156618, -24.65952944569304250, 1.056160979905700126 ) ) ;
#80321=CARTESIAN_POINT ( 'NONE',  ( 15.21843288076463629, 12.49332292251147614, 11.49999999999998934 ) ) ;
#80325=CARTESIAN_POINT ( 'NONE',  ( -17.29220519630379016, 15.29500218549028645, -1.500000000000002220 ) ) ;
#80327=EDGE_LOOP ( 'NONE', ( #84628, #75254, #18342, #11145 ) ) ;
#80328=CARTESIAN_POINT ( 'NONE',  ( -125.5228709571500900, -24.15516710230294706, 10.28746687063725318 ) ) ;
#80331=FACE_OUTER_BOUND ( 'NONE', #65544, .T. ) ;
#80332=CARTESIAN_POINT ( 'NONE',  ( -119.5228709571500616, -24.50216790748206819, 0.6166512839542566127 ) ) ;
#80334=CARTESIAN_POINT ( 'NONE',  ( -75.62287095715005592, -23.47596703998600631, 11.44779298504227860 ) ) ;
#80336=CARTESIAN_POINT ( 'NONE',  ( -15.85412420263326538, -12.13584807887712458, 11.49999999999998934 ) ) ;
#80337=LINE ( 'NONE', #10831, #40367 ) ;
#80338=CARTESIAN_POINT ( 'NONE',  ( -16.82575997001036328, 10.57904039763333159, -1.500000000000002220 ) ) ;
#80339=EDGE_LOOP ( 'NONE', ( #17254, #75088, #52180, #3057 ) ) ;
#80341=ADVANCED_FACE ( 'NONE', ( #86779 ), #54835, .T. ) ;
#80345=CARTESIAN_POINT ( 'NONE',  ( 14.06386034339543478, -15.33156129944631729, 11.49999999999999645 ) ) ;
#80348=CARTESIAN_POINT ( 'NONE',  ( 22.85402955525884394, -0.1436109537974766814, 11.49999999999999645 ) ) ;
#80350=DIRECTION ( 'NONE',  ( 0.000000000000000000, 0.9999999999976377785, 2.173523156925979128E-06 ) ) ;
#80351=CARTESIAN_POINT ( 'NONE',  ( -38.52287095715009713, -23.96127896942170921, -0.6493128930931766352 ) ) ;
#80353=VERTEX_POINT ( 'NONE', #28375 ) ;
#80354=EDGE_CURVE ( 'NONE', #61052, #11601, #69489, .T. ) ;
#80355=AXIS2_PLACEMENT_3D ( 'NONE', #49898, #65130, #11317 ) ;
#80356=CARTESIAN_POINT ( 'NONE',  ( -9.806399893892750796, 17.69452640759178408, 11.49999999999998934 ) ) ;
#80358=B_SPLINE_CURVE_WITH_KNOTS ( 'NONE', 3,
 ( #81607, #26817, #74485, #58767 ),
 .UNSPECIFIED., .F., .F.,
 ( 4, 4 ),
 ( 0.000000000000000000, 0.001846153846153858469 ),
 .UNSPECIFIED. ) ;
#80360=EDGE_CURVE ( 'NONE', #13954, #51364, #87649, .T. ) ;
#80362=B_SPLINE_CURVE_WITH_KNOTS ( 'NONE', 3,
 ( #27485, #66570, #35097, #12732 ),
 .UNSPECIFIED., .F., .F.,
 ( 4, 4 ),
 ( 0.000000000000000000, 9.999999999998897304E-05 ),
 .UNSPECIFIED. ) ;
#80363=CARTESIAN_POINT ( 'NONE',  ( -106.5895376238167387, -24.64898659630368627, 1.056161002820392270 ) ) ;
#80366=CARTESIAN_POINT ( 'NONE',  ( -79.56610238236960697, -25.31162433482952423, 5.317911015495634608 ) ) ;
#80367=CARTESIAN_POINT ( 'NONE',  ( -51.62287095715005592, -23.48783264082478084, -1.443836473390070596 ) ) ;
#80368=CARTESIAN_POINT ( 'NONE',  ( -7.547287378330592489, -18.53391252851691462, -1.500000000000002220 ) ) ;
#80370=CARTESIAN_POINT ( 'NONE',  ( 13.96602909953038640, 15.60522523583095200, 11.49999999999999645 ) ) ;
#80372=CARTESIAN_POINT ( 'NONE',  ( -124.6228709571500275, -23.72773821059535848, 11.05748984161097503 ) ) ;
#80373=CARTESIAN_POINT ( 'NONE',  ( 14.91618686576236108, -16.25093855066790738, 11.49999999999998934 ) ) ;
#80376=ORIENTED_EDGE ( 'NONE', *, *, #71672, .T. ) ;
#80377=CARTESIAN_POINT ( 'NONE',  ( -47.52287095715006160, -24.65952944569304606, 1.056160979905693686 ) ) ;
#80379=CARTESIAN_POINT ( 'NONE',  ( -50.55620429048340014, -24.99132157543166599, 2.256160258750668390 ) ) ;
#80381=CARTESIAN_POINT ( 'NONE',  ( -123.6228709571500559, -23.47596703998600631, 11.44779298504227860 ) ) ;
#80383=VERTEX_POINT ( 'NONE', #96897 ) ;
#80388=CARTESIAN_POINT ( 'NONE',  ( 12.01435098137705637, -16.61664908515649941, -1.500000000000002220 ) ) ;
#80390=CARTESIAN_POINT ( 'NONE',  ( -91.62287095715004170, -29.50250786944525672, 11.44777988621623344 ) ) ;
#80392=CARTESIAN_POINT ( 'NONE',  ( -96.55620429048339304, -24.66019654487199730, 8.947790411086124607 ) ) ;
#80393=CARTESIAN_POINT ( 'NONE',  ( -18.48265707593502327, -12.51853143457666562, 11.49999999999998934 ) ) ;
#80395=CARTESIAN_POINT ( 'NONE',  ( -104.6228709571500559, -24.64898659630529210, 1.056161002820829697 ) ) ;
#80398=CARTESIAN_POINT ( 'NONE',  ( -73.52287095715010423, -24.34917612406836795, 0.1852690917426544071 ) ) ;
#80399=CARTESIAN_POINT ( 'NONE',  ( -16.98601802344612111, -12.12340321765213069, 11.49999999999998934 ) ) ;
#80400=VERTEX_POINT ( 'NONE', #89786 ) ;
#80401=CARTESIAN_POINT ( 'NONE',  ( -86.62287095715004170, -29.50247984919015209, -1.443849546365051806 ) ) ;
#80402=VERTEX_POINT ( 'NONE', #34999 ) ;
#80404=CARTESIAN_POINT ( 'NONE',  ( -32.99388727629348494, -25.11010231571544082, 2.831122766524410750 ) ) ;
#80405=CARTESIAN_POINT ( 'NONE',  ( 17.02745815656931683, -12.38318283856952107, -1.500000000000002220 ) ) ;
#80406=ORIENTED_EDGE ( 'NONE', *, *, #35629, .T. ) ;
#80408=CARTESIAN_POINT ( 'NONE',  ( -78.62287095715007013, -23.48783264082478439, -1.443836473390065711 ) ) ;
#80409=CARTESIAN_POINT ( 'NONE',  ( -120.5892019400240827, -24.63419186844610920, 9.035850630976920428 ) ) ;
#80410=CARTESIAN_POINT ( 'NONE',  ( -86.63552721385731559, -23.96169478059713498, 10.65365249895717881 ) ) ;
#80411=CARTESIAN_POINT ( 'NONE',  ( -49.98701657552408761, -25.11998546545770594, 2.886102727180880567 ) ) ;
#80412=CARTESIAN_POINT ( 'NONE',  ( -21.53672441135761773, -2.854535511010750870, -1.500000000000002220 ) ) ;
#80413=CARTESIAN_POINT ( 'NONE',  ( -80.60699767246597958, -25.24759804226244597, 7.098405785189711992 ) ) ;
#80414=CARTESIAN_POINT ( 'NONE',  ( -5.617636847906702258, 21.56867655435222630, 11.49999999999999645 ) ) ;
#80416=CARTESIAN_POINT ( 'NONE',  ( -51.02375840103924531, -25.24728759653825350, 5.363929794370636550 ) ) ;
#80419=ORIENTED_EDGE ( 'NONE', *, *, #43262, .F. ) ;
#80422=ORIENTED_EDGE ( 'NONE', *, *, #18829, .F. ) ;
#80423=ADVANCED_FACE ( 'NONE', ( #89287 ), #73074, .T. ) ;
#80432=CARTESIAN_POINT ( 'NONE',  ( -130.5728709571500588, -24.35282530332708362, -0.01110346469458741055 ) ) ;
#80433=CARTESIAN_POINT ( 'NONE',  ( -16.90645664988545249, 14.66980924573920397, -1.500000000000002220 ) ) ;
#80437=CARTESIAN_POINT ( 'NONE',  ( -112.5161576296912074, -24.35071581493543391, 9.817618358456016381 ) ) ;
#80438=CARTESIAN_POINT ( 'NONE',  ( -101.5146321277283761, -24.15620529776628800, 10.23563542870660292 ) ) ;
#80439=FACE_OUTER_BOUND ( 'NONE', #77142, .T. ) ;
#80442=CARTESIAN_POINT ( 'NONE',  ( -130.5728709571500588, -24.26827793580486414, 9.960784317162948653 ) ) ;
#80443=CARTESIAN_POINT ( 'NONE',  ( 13.16580039582533423, -14.52177825760336205, 11.49999999999998934 ) ) ;
#80446=CARTESIAN_POINT ( 'NONE',  ( -10.19830463584622571, -18.94658877215714909, 11.49999999999998934 ) ) ;
#80447=CARTESIAN_POINT ( 'NONE',  ( -75.62287095715004170, -25.00182538069145366, 7.747789668545099317 ) ) ;
#80448=CARTESIAN_POINT ( 'NONE',  ( -81.01373513877602761, -25.31572665590242366, 5.057100087033362001 ) ) ;
#80451=CARTESIAN_POINT ( 'NONE',  ( 22.95104020007722667, -0.4190376320207603866, -1.500000000000002220 ) ) ;
#80454=CARTESIAN_POINT ( 'NONE',  ( -31.62287095715005236, -24.66019654487199020, 8.947790411086138818 ) ) ;
#80455=CARTESIAN_POINT ( 'NONE',  ( -49.52204961490906499, -23.48783264082477018, -1.443836473390094133 ) ) ;
#80456=CARTESIAN_POINT ( 'NONE',  ( 13.72940079880349984, -14.68433028913016791, 11.49999999999999645 ) ) ;
#80457=DIRECTION ( 'NONE',  ( -3.773278334453079030E-23, 0.9999999999976377785, 2.173523156925979128E-06 ) ) ;
#80458=CARTESIAN_POINT ( 'NONE',  ( -41.52287095715006870, -29.50250786944525672, 11.44777988621624232 ) ) ;
#80459=DIRECTION ( 'NONE',  ( 1.000000000000000000, 3.773278334444166432E-23, 8.201307841325785021E-29 ) ) ;
#80462=CARTESIAN_POINT ( 'NONE',  ( -15.05033210666397103, 12.90603908704162173, -1.500000000000002220 ) ) ;
#80463=DIRECTION ( 'NONE',  ( -3.773278334453079030E-23, 0.9999999999976377785, 2.173523156925979128E-06 ) ) ;
#80464=CARTESIAN_POINT ( 'NONE',  ( -18.32884136524465291, -7.267937366463995907, -1.500000000000002220 ) ) ;
#80468=DIRECTION ( 'NONE',  ( 3.773278334444166432E-23, -1.000000000000000000, 0.000000000000000000 ) ) ;
#80469=CARTESIAN_POINT ( 'NONE',  ( -82.62287095715005592, -29.50248528299804818, 1.056150453629038477 ) ) ;
#80470=CARTESIAN_POINT ( 'NONE',  ( 16.46467569749531634, 12.45148609503053017, 11.49999999999999645 ) ) ;
#80471=PLANE ( 'NONE',  #67557 ) ;
#80472=CARTESIAN_POINT ( 'NONE',  ( -19.30582015231555104, -11.89196067722419237, 11.49999999999999645 ) ) ;
#80473=VERTEX_POINT ( 'NONE', #72569 ) ;
#80474=CARTESIAN_POINT ( 'NONE',  ( -69.63000454671555417, -25.12219088186380134, 6.841411392149890247 ) ) ;
#80475=DIRECTION ( 'NONE',  ( -3.773278334453079618E-23, 0.9999999999976377785, 2.173523156925979975E-06 ) ) ;
#80476=EDGE_CURVE ( 'NONE', #36980, #47332, #47753, .T. ) ;
#80477=CARTESIAN_POINT ( 'NONE',  ( -110.5228709571500616, -25.00158670708909625, 2.256160236439166411 ) ) ;
#80479=VECTOR ( 'NONE', #60123, 1000.000000000000114 ) ;
#80482=CARTESIAN_POINT ( 'NONE',  ( -19.58686714514938387, 11.73587220785771379, 11.49999999999998934 ) ) ;
#80484=CARTESIAN_POINT ( 'NONE',  ( -96.51075182989580981, -24.34968618360933945, 0.1864209137778868874 ) ) ;
#80485=CARTESIAN_POINT ( 'NONE',  ( -82.55075552779136672, -24.15620529776628089, 10.23563542870660825 ) ) ;
#80487=CARTESIAN_POINT ( 'NONE',  ( -17.89120377161202313, 13.61666483413312712, 11.49999999999999645 ) ) ;
#80489=CARTESIAN_POINT ( 'NONE',  ( -99.62287095715005592, -24.65952944569304961, 1.056160979905702124 ) ) ;
#80490=CARTESIAN_POINT ( 'NONE',  ( -11.46427080702723522, -18.74017919159951973, -1.500000000000002220 ) ) ;
#80492=CARTESIAN_POINT ( 'NONE',  ( -125.7765869487822670, -25.31326647857923007, 3.500947721614712016 ) ) ;
#80494=CARTESIAN_POINT ( 'NONE',  ( -111.5203660093640678, -23.73766607897670511, -1.055555164236450461 ) ) ;
#80496=ORIENTED_EDGE ( 'NONE', *, *, #3878, .F. ) ;
#80497=CARTESIAN_POINT ( 'NONE',  ( -48.55325661869351705, -23.96169478059713143, 10.65365249895718236 ) ) ;
#80498=CARTESIAN_POINT ( 'NONE',  ( -107.5228709571500758, -23.47596703998600631, 11.44779298504228038 ) ) ;
#80499=VERTEX_POINT ( 'NONE', #91277 ) ;
#80500=VECTOR ( 'NONE', #30738, 1000.000000000000114 ) ;
#80501=CARTESIAN_POINT ( 'NONE',  ( -54.65831064146149743, -23.48786465467240347, 11.44779295918255357 ) ) ;
#80502=CARTESIAN_POINT ( 'NONE',  ( 20.32696876622996029, 2.630761579057304900, 11.49999999999998934 ) ) ;
#80503=EDGE_LOOP ( 'NONE', ( #7299, #63168, #42740, #7843 ) ) ;
#80506=ORIENTED_EDGE ( 'NONE', *, *, #73115, .F. ) ;
#80507=CARTESIAN_POINT ( 'NONE',  ( -84.62287095715004170, -24.51283580621365132, 0.6167428607019797004 ) ) ;
#80508=CARTESIAN_POINT ( 'NONE',  ( 6.910522817300494225, 22.03692736239173300, 11.49999999999998934 ) ) ;
#80510=EDGE_CURVE ( 'NONE', #48044, #6944, #61042, .T. ) ;
#80511=CARTESIAN_POINT ( 'NONE',  ( -18.95781532540867076, -7.450117396690965066, -1.500000000000002220 ) ) ;
#80512=VERTEX_POINT ( 'NONE', #61345 ) ;
#80513=CARTESIAN_POINT ( 'NONE',  ( -71.25388481961385878, -25.09966334678765421, 7.231536832813914906 ) ) ;
#80514=CARTESIAN_POINT ( 'NONE',  ( -29.49548802756975974, -24.06924278478361856, 10.23563548314527338 ) ) ;
#80517=CARTESIAN_POINT ( 'NONE',  ( -71.53177174497976409, -25.25855234727440646, 6.885843230737062726 ) ) ;
#80519=CARTESIAN_POINT ( 'NONE',  ( -29.05456498926589504, -24.76881090259380613, 3.361080071346441933 ) ) ;
#80520=CARTESIAN_POINT ( 'NONE',  ( -49.11003834631243592, -25.31573659134376442, 4.144493024849963625 ) ) ;
#80521=ORIENTED_EDGE ( 'NONE', *, *, #1110, .F. ) ;
#80522=CARTESIAN_POINT ( 'NONE',  ( -19.91680486407696904, 5.911688619927280008, -1.500000000000002220 ) ) ;
#80523=VERTEX_POINT ( 'NONE', #21748 ) ;
#80525=CARTESIAN_POINT ( 'NONE',  ( -125.5196044704536007, -24.83618233451450763, 1.606449574219537046 ) ) ;
#80527=LINE ( 'NONE', #95254, #8237 ) ;
#80528=DIRECTION ( 'NONE',  ( 0.000000000000000000, -2.173523156925980399E-06, 0.9999999999976378895 ) ) ;
#80531=CARTESIAN_POINT ( 'NONE',  ( -29.62287095715005947, -23.87211438191165058, -0.6496301950016380999 ) ) ;
#80532=FACE_OUTER_BOUND ( 'NONE', #71097, .T. ) ;
#80533=CARTESIAN_POINT ( 'NONE',  ( -70.55843555340263151, -25.24515045242101507, 5.327474807685200098 ) ) ;
#80534=ADVANCED_FACE ( 'NONE', ( #77038 ), #6545, .T. ) ;
#80535=CARTESIAN_POINT ( 'NONE',  ( 5.627179592841175193, 21.36305014179116668, 11.49999999999999645 ) ) ;
#80536=ORIENTED_EDGE ( 'NONE', *, *, #35868, .F. ) ;
#80537=CARTESIAN_POINT ( 'NONE',  ( -101.5228709571500758, -23.47596703998600631, 11.44779298504228215 ) ) ;
#80538=CARTESIAN_POINT ( 'NONE',  ( 22.41689761077644860, -2.907977976681301424, 11.49999999999998934 ) ) ;
#80542=EDGE_CURVE ( 'NONE', #19840, #66017, #97340, .T. ) ;
#80543=EDGE_LOOP ( 'NONE', ( #92962, #65448, #5663, #53254 ) ) ;
#80544=VECTOR ( 'NONE', #33757, 1000.000000000000114 ) ;
#80545=DIRECTION ( 'NONE',  ( 0.000000000000000000, -0.9999999999976377785, -2.173523156925979128E-06 ) ) ;
#80547=CARTESIAN_POINT ( 'NONE',  ( -101.5468792378191978, -29.50249654204571215, 6.236241424690079249 ) ) ;
#80548=ORIENTED_EDGE ( 'NONE', *, *, #64838, .T. ) ;
#80549=CARTESIAN_POINT ( 'NONE',  ( -10.65520286329281596, -18.28862552182625123, -1.500000000000002220 ) ) ;
#80550=FACE_OUTER_BOUND ( 'NONE', #31693, .T. ) ;
#80551=LINE ( 'NONE', #42510, #67034 ) ;
#80552=CARTESIAN_POINT ( 'NONE',  ( -40.49165087243459737, -25.29352311369862605, 5.543942880681965946 ) ) ;
#80553=CARTESIAN_POINT ( 'NONE',  ( -19.85906585229243504, 9.992431322412627992, -1.500000000000002220 ) ) ;
#80554=DIRECTION ( 'NONE',  ( 0.000000000000000000, -2.173523156925980399E-06, 0.9999999999976378895 ) ) ;
#80555=B_SPLINE_CURVE_WITH_KNOTS ( 'NONE', 3,
 ( #15097, #76482, #7478, #60294, #29322, #6988 ),
 .UNSPECIFIED., .F., .F.,
 ( 4, 2, 4 ),
 ( 0.000000000000000000, 0.001380764517853254672, 0.002761529035706509344 ),
 .UNSPECIFIED. ) ;
#80556=ORIENTED_EDGE ( 'NONE', *, *, #37843, .T. ) ;
#80557=CARTESIAN_POINT ( 'NONE',  ( -110.5562042904834072, -23.47596703998600631, 11.44779298504227683 ) ) ;
#80559=CARTESIAN_POINT ( 'NONE',  ( -36.53861774053764577, -24.35071581493542325, 9.817618358456030592 ) ) ;
#80560=B_SPLINE_CURVE_WITH_KNOTS ( 'NONE', 3,
 ( #37772, #30149, #98660, #75823 ),
 .UNSPECIFIED., .F., .F.,
 ( 4, 4 ),
 ( 0.4107933374670430515, 0.4197997687391585853 ),
 .UNSPECIFIED. ) ;
#80561=DIRECTION ( 'NONE',  ( -3.773278334453079618E-23, 0.9999999999976377785, 2.173523156925979975E-06 ) ) ;
#80562=CARTESIAN_POINT ( 'NONE',  ( 0.2958748881272694198, 19.47992435465491212, -1.500000000000002220 ) ) ;
#80563=CARTESIAN_POINT ( 'NONE',  ( 15.25824911148008844, 15.06768998368162471, 11.49999999999998934 ) ) ;
#80566=CARTESIAN_POINT ( 'NONE',  ( -77.55884306925648275, -23.73766607897670156, -1.055555164236459564 ) ) ;
#80567=CARTESIAN_POINT ( 'NONE',  ( 19.47892149737544187, 11.75266795981601753, -1.500000000000002220 ) ) ;
#80568=ADVANCED_FACE ( 'NONE', ( #99866 ), #86434, .T. ) ;
#80570=CARTESIAN_POINT ( 'NONE',  ( -98.62740225175618036, -24.34968618360934656, 0.1864209137778829184 ) ) ;
#80572=CARTESIAN_POINT ( 'NONE',  ( -6.132916590032589710, 18.96384228413732842, 11.49999999999999645 ) ) ;
#80573=CARTESIAN_POINT ( 'NONE',  ( -69.52287095715006160, -24.65952944569304606, 1.056160979905697239 ) ) ;
#80574=EDGE_CURVE ( 'NONE', #30754, #14223, #79186, .T. ) ;
#80576=FACE_OUTER_BOUND ( 'NONE', #58989, .T. ) ;
#80577=CARTESIAN_POINT ( 'NONE',  ( -48.53099033229920423, -24.65952944569304606, 1.056160979905697461 ) ) ;
#80578=EDGE_LOOP ( 'NONE', ( #51061, #11389, #55839, #35452 ) ) ;
#80579=DIRECTION ( 'NONE',  ( 3.773278334444167608E-23, -1.000000000000000000, 0.000000000000000000 ) ) ;
#80580=CARTESIAN_POINT ( 'NONE',  ( -31.21621552302040925, -25.31558585043574183, 4.997857581739419075 ) ) ;
#80581=CARTESIAN_POINT ( 'NONE',  ( -9.282276271697774916, -19.63344595494797673, 11.49999999999998934 ) ) ;
#80582=ADVANCED_FACE ( 'NONE', ( #73325 ), #93703, .T. ) ;
#80583=CARTESIAN_POINT ( 'NONE',  ( -51.33976102265904018, -25.09150690715527787, 7.330714471490653139 ) ) ;
#80584=CARTESIAN_POINT ( 'NONE',  ( 6.866622826037362515, -18.30913693658520103, -1.500000000000002220 ) ) ;
#80589=DIRECTION ( 'NONE',  ( -3.773278334453079618E-23, 0.9999999999976377785, 2.173523156925979552E-06 ) ) ;
#80590=CARTESIAN_POINT ( 'NONE',  ( -18.43012528856881715, -8.789534013050598560, 11.49999999999999645 ) ) ;
#80591=CARTESIAN_POINT ( 'NONE',  ( -110.5562042904833930, -23.48783264082478794, -1.443836473390060160 ) ) ;
#80593=ORIENTED_EDGE ( 'NONE', *, *, #73053, .F. ) ;
#80597=EDGE_CURVE ( 'NONE', #94573, #39942, #14935, .T. ) ;
#80598=CARTESIAN_POINT ( 'NONE',  ( -109.5922554486619021, -23.96119346886880663, -0.6495511937832053606 ) ) ;
#80599=VERTEX_POINT ( 'NONE', #54232 ) ;
#80602=CARTESIAN_POINT ( 'NONE',  ( 11.31314246093949727, 19.96360691973900359, 11.49999999999999645 ) ) ;
#80603=CARTESIAN_POINT ( 'NONE',  ( 2.720868037236281012, -22.60253418658637869, 11.49999999999998934 ) ) ;
#80604=CARTESIAN_POINT ( 'NONE',  ( -110.5895321101819917, -24.52399227489125266, 9.353111116836528183 ) ) ;
#80607=CARTESIAN_POINT ( 'NONE',  ( -90.49854698813747689, -25.00158670708910336, 2.256160236439220146 ) ) ;
#80609=CARTESIAN_POINT ( 'NONE',  ( -54.52287095715011844, -23.73907113216988307, -1.053371485793257456 ) ) ;
#80610=CARTESIAN_POINT ( 'NONE',  ( -93.62287095715007013, -23.47596703998600631, 11.44779298504227860 ) ) ;
#80611=CARTESIAN_POINT ( 'NONE',  ( 6.672210613628693388, 20.84999943921648935, 11.49999999999998934 ) ) ;
#80612=ADVANCED_FACE ( 'NONE', ( #39495 ), #932, .T. ) ;
#80615=CARTESIAN_POINT ( 'NONE',  ( -115.6228709571500701, -24.92579138211019796, 1.929029949965668456 ) ) ;
#80616=DIRECTION ( 'NONE',  ( 3.773278334444165844E-23, -1.000000000000000000, 0.000000000000000000 ) ) ;
#80618=ORIENTED_EDGE ( 'NONE', *, *, #74619, .T. ) ;
#80620=CARTESIAN_POINT ( 'NONE',  ( -6.584652030910324250, 19.34213596296284265, 11.49999999999998934 ) ) ;
#80623=VERTEX_POINT ( 'NONE', #79044 ) ;
#80624=CARTESIAN_POINT ( 'NONE',  ( 22.51966570110743149, 4.691836548664650053, 11.49999999999998934 ) ) ;
#80625=CARTESIAN_POINT ( 'NONE',  ( -105.6228709571500559, -23.48783264082479150, -1.443836473390060160 ) ) ;
#80626=EDGE_CURVE ( 'NONE', #85746, #35212, #50013, .T. ) ;
#80627=CARTESIAN_POINT ( 'NONE',  ( -1.055277534996966970, 20.15608268182561247, -1.500000000000002220 ) ) ;
#80628=ORIENTED_EDGE ( 'NONE', *, *, #12786, .F. ) ;
#80629=CARTESIAN_POINT ( 'NONE',  ( -67.62287095715005592, -23.73934037231756733, 11.05740245334329330 ) ) ;
#80631=CARTESIAN_POINT ( 'NONE',  ( -34.58953762381672448, -24.64965694238406613, 8.947790433994663672 ) ) ;
#80634=CARTESIAN_POINT ( 'NONE',  ( -98.62287095715009855, -23.96177878511308990, 10.65340807706329684 ) ) ;
#80635=CARTESIAN_POINT ( 'NONE',  ( -53.59900155969933877, -23.96169478059712787, 10.65365249895718591 ) ) ;
#80636=CARTESIAN_POINT ( 'NONE',  ( 11.27511198983438412, 18.17944245918264912, 11.49999999999999645 ) ) ;
#80637=ORIENTED_EDGE ( 'NONE', *, *, #96338, .F. ) ;
#80639=VERTEX_POINT ( 'NONE', #90042 ) ;
#80640=CARTESIAN_POINT ( 'NONE',  ( 22.17158117043571863, -1.905908075979310334, -1.500000000000002220 ) ) ;
#80641=B_SPLINE_CURVE_WITH_KNOTS ( 'NONE', 3,
 ( #12157, #41130, #58358, #88300, #65485, #89794 ),
 .UNSPECIFIED., .F., .F.,
 ( 4, 2, 4 ),
 ( 1.570887131794176733E-05, 0.001396322306279758037, 0.002776935741241574537 ),
 .UNSPECIFIED. ) ;
#80642=CARTESIAN_POINT ( 'NONE',  ( 20.01179378540625819, 5.277757631783551950, -1.500000000000002220 ) ) ;
#80646=CARTESIAN_POINT ( 'NONE',  ( -68.92155128426668398, -25.30060019737137367, 6.009288023823078362 ) ) ;
#80647=ORIENTED_EDGE ( 'NONE', *, *, #98783, .T. ) ;
#80648=CARTESIAN_POINT ( 'NONE',  ( -78.94303308397304875, -25.27645460285955181, 5.977536667781793156 ) ) ;
#80650=EDGE_LOOP ( 'NONE', ( #24105, #46162, #23201, #24693 ) ) ;
#80652=CARTESIAN_POINT ( 'NONE',  ( 5.463070048063013218, -20.23478146675526190, -1.500000000000002220 ) ) ;
#80653=CARTESIAN_POINT ( 'NONE',  ( 1.548332177993611225, -21.85883989728069565, 11.49999999999999645 ) ) ;
#80654=CARTESIAN_POINT ( 'NONE',  ( -107.6228709571500985, -23.96177878511308634, 10.65340807706329507 ) ) ;
#80655=CARTESIAN_POINT ( 'NONE',  ( -6.794891441663577503, 21.43730618243864683, -1.500000000000002220 ) ) ;
#80656=CARTESIAN_POINT ( 'NONE',  ( 18.03207908435136986, 10.65457695745678457, 11.49999999999998934 ) ) ;
#80657=PLANE ( 'NONE',  #53023 ) ;
#80659=CARTESIAN_POINT ( 'NONE',  ( -91.52287095715006160, -24.64965694238575011, 8.947790433994196491 ) ) ;
#80662=ORIENTED_EDGE ( 'NONE', *, *, #91456, .T. ) ;
#80663=CARTESIAN_POINT ( 'NONE',  ( -51.52287095715006870, -23.48786465467241058, 11.44779295918255002 ) ) ;
#80665=CARTESIAN_POINT ( 'NONE',  ( 14.52366289275476419, -15.72616519631134580, -1.500000000000002220 ) ) ;
#80667=CARTESIAN_POINT ( 'NONE',  ( -26.09992617429942285, -24.95874029368170000, 5.209038662095228922 ) ) ;
#80668=CARTESIAN_POINT ( 'NONE',  ( 19.72786461798894209, 7.474574171381012100, -1.500000000000002220 ) ) ;
#80669=CARTESIAN_POINT ( 'NONE',  ( -30.42619003775230269, -24.66229007638825621, 8.908675929220798650 ) ) ;
#80672=CARTESIAN_POINT ( 'NONE',  ( -101.5575534224985574, -23.73766607897671221, -1.055555164236452237 ) ) ;
#80673=CARTESIAN_POINT ( 'NONE',  ( -129.6237316671312101, -23.96169478059714564, 10.65365249895717348 ) ) ;
#80674=CARTESIAN_POINT ( 'NONE',  ( -18.71521858236628333, -11.60751834597489740, -1.500000000000002220 ) ) ;
#80676=CARTESIAN_POINT ( 'NONE',  ( -116.5544677183481639, -24.15543982623908548, -0.2315651400026407236 ) ) ;
#80677=DIRECTION ( 'NONE',  ( -3.773278334453079618E-23, 0.9999999999976377785, 2.173523156925979975E-06 ) ) ;
#80680=CARTESIAN_POINT ( 'NONE',  ( -62.65464089196193243, -23.48786465467241413, 11.44779295918255002 ) ) ;
#80681=B_SPLINE_CURVE_WITH_KNOTS ( 'NONE', 3,
 ( #3152, #12227, #57444, #67050, #12726, #27480 ),
 .UNSPECIFIED., .F., .F.,
 ( 4, 2, 4 ),
 ( 0.000000000000000000, 0.001380764517853249034, 0.002761529035706498068 ),
 .UNSPECIFIED. ) ;
#80682=CARTESIAN_POINT ( 'NONE',  ( -25.53616547081472987, -24.90994025867288642, 4.571154658487995626 ) ) ;
#80683=CARTESIAN_POINT ( 'NONE',  ( -79.62287095715005592, -29.50248528299804818, 1.056150453629038477 ) ) ;
#80684=CARTESIAN_POINT ( 'NONE',  ( 19.59546714036918758, 8.467717511154198462, 11.49999999999998934 ) ) ;
#80685=CARTESIAN_POINT ( 'NONE',  ( -97.62287095715001328, -24.51387760970724372, 9.387446482453411178 ) ) ;
#80686=CARTESIAN_POINT ( 'NONE',  ( -51.94857094028245115, -25.30060005375479903, 6.009289253917323492 ) ) ;
#80687=CARTESIAN_POINT ( 'NONE',  ( -0.1447603125146491310, -21.17596399598531676, 11.48393099501409687 ) ) ;
#80688=CARTESIAN_POINT ( 'NONE',  ( -67.58953762381669605, -24.66019654487198665, 8.947790411086131712 ) ) ;
#80689=CARTESIAN_POINT ( 'NONE',  ( -16.99934442671578694, -14.85117937636706031, -1.500000000000002220 ) ) ;
#80690=EDGE_CURVE ( 'NONE', #47965, #2532, #37956, .T. ) ;
#80691=B_SPLINE_CURVE_WITH_KNOTS ( 'NONE', 3,
 ( #80625, #58792, #49696, #33955 ),
 .UNSPECIFIED., .F., .F.,
 ( 4, 4 ),
 ( 0.000000000000000000, 9.999999999996123101E-05 ),
 .UNSPECIFIED. ) ;
#80692=B_SPLINE_SURFACE_WITH_KNOTS ( 'NONE', 3, 3, ( 
 ( #15287, #29515, #46757, #77679 ),
 ( #69595, #23906, #61985, #14286 ),
 ( #60494, #53871, #91411, #31019 ),
 ( #46252, #30014, #92412, #92911 ),
 ( #77179, #31520, #8191, #39132 ),
 ( #22883, #23388, #22390, #76672 ),
 ( #62485, #7685, #53374, #93411 ) ),
 .UNSPECIFIED., .F., .F., .F.,
 ( 4, 3, 4 ),
 ( 4, 4 ),
 ( 0.3409880801055691912, 0.5103009464560217534, 0.6796138128064742601 ),
 ( 0.3860895931267444570, 0.4170344922427780543 ),
 .UNSPECIFIED. ) ;
#80693=CARTESIAN_POINT ( 'NONE',  ( -47.52287095715004028, -24.51283580621461411, 0.6167428607048329736 ) ) ;
#80696=CARTESIAN_POINT ( 'NONE',  ( -79.58816022331352258, -24.34968618360933945, 0.1864209137778814473 ) ) ;
#80697=CARTESIAN_POINT ( 'NONE',  ( 0.5484783294719396407, -19.75002165935583776, 11.49999999999999645 ) ) ;
#80698=CARTESIAN_POINT ( 'NONE',  ( -49.52287095715006870, -23.72747288104469732, -1.053458166803227236 ) ) ;
#80699=CARTESIAN_POINT ( 'NONE',  ( -67.56550939864793293, -23.48783264082477018, -1.443836473390094799 ) ) ;
#80700=B_SPLINE_CURVE_WITH_KNOTS ( 'NONE', 3,
 ( #69509, #93330, #42616, #86228 ),
 .UNSPECIFIED., .F., .F.,
 ( 4, 4 ),
 ( 0.000000000000000000, 0.0001000000000000028644 ),
 .UNSPECIFIED. ) ;
#80701=VERTEX_POINT ( 'NONE', #75796 ) ;
#80702=CARTESIAN_POINT ( 'NONE',  ( -117.5228709571500758, -24.65952944569305316, 1.056160979905705899 ) ) ;
#80703=CARTESIAN_POINT ( 'NONE',  ( -29.77605907665351737, -25.26026821586171422, 4.091748813052181966 ) ) ;
#80704=CARTESIAN_POINT ( 'NONE',  ( -100.4426124108961176, -25.12268565766455808, 7.101635559697120570 ) ) ;
#80705=EDGE_CURVE ( 'NONE', #61817, #40347, #1660, .T. ) ;
#80706=CARTESIAN_POINT ( 'NONE',  ( -15.70146493180990888, -14.86199287721409590, 11.49999999999998934 ) ) ;
#80707=EDGE_CURVE ( 'NONE', #14386, #37312, #43868, .T. ) ;
#80708=CARTESIAN_POINT ( 'NONE',  ( -42.62287095715004881, -29.50248528299804818, 1.056150453629031594 ) ) ;
#80710=CARTESIAN_POINT ( 'NONE',  ( -65.62287095715005592, -24.99156045073393173, 7.747789690856161648 ) ) ;
#80711=EDGE_CURVE ( 'NONE', #62807, #42765, #65729, .T. ) ;
#80712=CARTESIAN_POINT ( 'NONE',  ( -0.1490749075164066184, -21.12010817310450861, 11.44779298504228038 ) ) ;
#80714=CARTESIAN_POINT ( 'NONE',  ( -18.42202159362721048, -7.168033771007030097, -1.500000000000002220 ) ) ;
#80716=EDGE_CURVE ( 'NONE', #47332, #79914, #79105, .T. ) ;
#80717=CARTESIAN_POINT ( 'NONE',  ( 20.05691770114479766, 3.104179615465487707, 11.49999999999999645 ) ) ;
#80720=ORIENTED_EDGE ( 'NONE', *, *, #83499, .T. ) ;
#80722=CARTESIAN_POINT ( 'NONE',  ( -110.6228709571500559, -24.99132157543166954, 2.256160258750667502 ) ) ;
#80724=LINE ( 'NONE', #88842, #46903 ) ;
#80726=CARTESIAN_POINT ( 'NONE',  ( -103.6228709571500701, -24.33927499327855060, 9.819080762295817166 ) ) ;
#80727=CARTESIAN_POINT ( 'NONE',  ( -86.52287095715006160, -24.66019654487199375, 8.947790411086119278 ) ) ;
#80728=CARTESIAN_POINT ( 'NONE',  ( -5.935188749463110369, 19.13178230186815298, -1.500000000000002220 ) ) ;
#80729=EDGE_CURVE ( 'NONE', #66603, #17632, #6294, .T. ) ;
#80730=CARTESIAN_POINT ( 'NONE',  ( -76.62287095715007013, -24.64898659630367916, 1.056161002820826145 ) ) ;
#80731=VERTEX_POINT ( 'NONE', #89540 ) ;
#80732=ADVANCED_FACE ( 'NONE', ( #50990 ), #13397, .T. ) ;
#80733=AXIS2_PLACEMENT_3D ( 'NONE', #15438, #62636, #79339 ) ;
#80738=CARTESIAN_POINT ( 'NONE',  ( -73.55409649099257763, -23.96119346886880663, -0.6495511937832116889 ) ) ;
#80739=EDGE_CURVE ( 'NONE', #16861, #100167, #77821, .T. ) ;
#80741=CARTESIAN_POINT ( 'NONE',  ( -49.98787894874461557, -25.19317122439448653, 3.352862466847235545 ) ) ;
#80742=ORIENTED_EDGE ( 'NONE', *, *, #74867, .F. ) ;
#80743=CARTESIAN_POINT ( 'NONE',  ( 9.809556900635294951, 17.81656380412256269, -1.500000000000002220 ) ) ;
#80745=CARTESIAN_POINT ( 'NONE',  ( -5.713817535623205046, 22.21719745612757535, -1.500000000000002220 ) ) ;
#80746=EDGE_CURVE ( 'NONE', #19840, #80599, #28145, .T. ) ;
#80748=CARTESIAN_POINT ( 'NONE',  ( -127.6245371603278755, -23.73791477778912551, 11.05961554403169345 ) ) ;
#80749=VERTEX_POINT ( 'NONE', #11913 ) ;
#80750=CARTESIAN_POINT ( 'NONE',  ( -49.10837252249681484, -25.27212926941085769, 4.099823236261497250 ) ) ;
#80752=B_SPLINE_CURVE_WITH_KNOTS ( 'NONE', 3,
 ( #83962, #60153, #75843, #45414 ),
 .UNSPECIFIED., .F., .F.,
 ( 4, 4 ),
 ( 0.4891186356891960019, 0.4901193827299611394 ),
 .UNSPECIFIED. ) ;
#80753=CARTESIAN_POINT ( 'NONE',  ( -49.27841808360716414, -25.12215218622909418, 6.176813154470331746 ) ) ;
#80754=B_SPLINE_CURVE_WITH_KNOTS ( 'NONE', 3,
 ( #48502, #87044, #63741, #55109 ),
 .UNSPECIFIED., .F., .F.,
 ( 4, 4 ),
 ( 0.000000000000000000, 9.999999999998206125E-05 ),
 .UNSPECIFIED. ) ;
#80755=CARTESIAN_POINT ( 'NONE',  ( -66.62287095715005592, -24.64965695001468404, 8.947790433994184056 ) ) ;
#80756=CARTESIAN_POINT ( 'NONE',  ( -19.98547761299008130, 7.154247560337752887, 11.49999999999999645 ) ) ;
#80757=CARTESIAN_POINT ( 'NONE',  ( -5.973063517705734071, 21.31661749205449041, 11.49999999999998934 ) ) ;
#80759=CARTESIAN_POINT ( 'NONE',  ( 13.11803791274172681, -15.88952355948706341, 11.49999999999998934 ) ) ;
#80760=ORIENTED_EDGE ( 'NONE', *, *, #92459, .T. ) ;
#80762=VERTEX_POINT ( 'NONE', #20510 ) ;
#80763=DIRECTION ( 'NONE',  ( 0.000000000000000000, 2.173523156925980399E-06, -0.9999999999976378895 ) ) ;
#80764=DIRECTION ( 'NONE',  ( 0.000000000000000000, -0.9999999999976377785, -2.173523156925979975E-06 ) ) ;
#80765=ORIENTED_EDGE ( 'NONE', *, *, #17952, .T. ) ;
#80771=CARTESIAN_POINT ( 'NONE',  ( -5.954758479537505700, 19.85987847461844424, -1.500000000000002220 ) ) ;
#80772=CARTESIAN_POINT ( 'NONE',  ( 14.13103794885040898, -16.47871000921984219, 11.49999999999999645 ) ) ;
#80773=ORIENTED_EDGE ( 'NONE', *, *, #43144, .T. ) ;
#80775=CARTESIAN_POINT ( 'NONE',  ( -105.5228709571500758, -23.47593901973090524, -1.443836447538996426 ) ) ;
#80776=CARTESIAN_POINT ( 'NONE',  ( 22.22467975111640470, 2.813832150844377100, 11.49999999999998934 ) ) ;
#80777=AXIS2_PLACEMENT_3D ( 'NONE', #19062, #41927, #80468 ) ;
#80778=B_SPLINE_CURVE_WITH_KNOTS ( 'NONE', 3,
 ( #8323, #32155, #47396, #85439 ),
 .UNSPECIFIED., .F., .F.,
 ( 4, 4 ),
 ( 0.000000000000000000, 1.000000000000000000 ),
 .UNSPECIFIED. ) ;
#80779=CARTESIAN_POINT ( 'NONE',  ( -79.62287095715004170, -24.65952944569304606, 1.056160979905697461 ) ) ;
#80780=CARTESIAN_POINT ( 'NONE',  ( -121.5228709571500616, -24.64965694238408034, 8.947790433994191162 ) ) ;
#80782=CARTESIAN_POINT ( 'NONE',  ( -32.52287095715006160, -24.65952944569304606, 1.056160979905690134 ) ) ;
#80783=CARTESIAN_POINT ( 'NONE',  ( -119.4728709548940628, -25.21112548385455199, 2.000950964958121414 ) ) ;
#80784=ORIENTED_EDGE ( 'NONE', *, *, #13828, .F. ) ;
#80785=ORIENTED_EDGE ( 'NONE', *, *, #95524, .T. ) ;
#80786=CARTESIAN_POINT ( 'NONE',  ( -38.62287095715005592, -29.50248528299804818, 1.056150453629031594 ) ) ;
#80787=VERTEX_POINT ( 'NONE', #92520 ) ;
#80788=CARTESIAN_POINT ( 'NONE',  ( 12.23393567461250697, 17.36540613969008007, -1.500000000000002220 ) ) ;
#80789=B_SPLINE_CURVE_WITH_KNOTS ( 'NONE', 3,
 ( #22744, #53728, #98882, #84659 ),
 .UNSPECIFIED., .F., .F.,
 ( 4, 4 ),
 ( 0.9904932114349886962, 1.000000000000000000 ),
 .UNSPECIFIED. ) ;
#80790=VERTEX_POINT ( 'NONE', #23491 ) ;
#80791=CARTESIAN_POINT ( 'NONE',  ( -88.62358598722710212, -24.65952944569304606, 1.056160979905700126 ) ) ;
#80792=CARTESIAN_POINT ( 'NONE',  ( 4.989390281198801347, -21.28523531580253803, 11.49999999999998934 ) ) ;
#80793=DIRECTION ( 'NONE',  ( 0.000000000000000000, -0.9999999999976377785, -2.173523156925979975E-06 ) ) ;
#80796=CARTESIAN_POINT ( 'NONE',  ( -35.62287095715006302, -24.91544648472620338, 1.928969306349229695 ) ) ;
#80797=CARTESIAN_POINT ( 'NONE',  ( 11.25260618158950621, 18.78031238747207610, -1.500000000000002220 ) ) ;
#80800=CARTESIAN_POINT ( 'NONE',  ( -65.62287095715004170, -24.92579138211018375, 1.929029949965667123 ) ) ;
#80801=CARTESIAN_POINT ( 'NONE',  ( -73.55620429048339304, -24.64898659630528854, 1.056161002820822592 ) ) ;
#80802=ORIENTED_EDGE ( 'NONE', *, *, #5680, .F. ) ;
#80805=ORIENTED_EDGE ( 'NONE', *, *, #88971, .T. ) ;
#80807=CARTESIAN_POINT ( 'NONE',  ( -20.48352739510140452, -22.69081920706126354, -1.443836447538997314 ) ) ;
#80808=CARTESIAN_POINT ( 'NONE',  ( -20.90244970016518877, -3.954922567530639199, -1.500000000000002220 ) ) ;
#80809=CARTESIAN_POINT ( 'NONE',  ( -118.6228709571500559, -29.50250786944525672, 11.44777988621622811 ) ) ;
#80811=CARTESIAN_POINT ( 'NONE',  ( -85.49691536098328015, -24.92564183028979485, 1.928384488918252204 ) ) ;
#80812=CARTESIAN_POINT ( 'NONE',  ( -68.53708757987610056, -24.65952944569304606, 1.056160979905701236 ) ) ;
#80813=CARTESIAN_POINT ( 'NONE',  ( 10.09180897563621926, 16.61094848277074476, -1.500000000000002220 ) ) ;
#80814=CARTESIAN_POINT ( 'NONE',  ( -45.53467254122168839, -24.63355581998386867, 0.9682620441943888823 ) ) ;
#80815=ORIENTED_EDGE ( 'NONE', *, *, #82193, .T. ) ;
#80816=EDGE_CURVE ( 'NONE', #27205, #1265, #45156, .T. ) ;
#80817=CARTESIAN_POINT ( 'NONE',  ( 11.58774116221665729, 15.72987433093905096, 11.49999999999999645 ) ) ;
#80820=CARTESIAN_POINT ( 'NONE',  ( -116.5228709571500616, -23.48786465467241769, 11.44779295918253759 ) ) ;
#80823=CARTESIAN_POINT ( 'NONE',  ( -97.62287095715005592, -24.64898659630367916, 1.056161002820829697 ) ) ;
#80824=CARTESIAN_POINT ( 'NONE',  ( -89.58846763882705488, -24.34968618360933945, 0.1864209137778942982 ) ) ;
#80825=EDGE_CURVE ( 'NONE', #51581, #75656, #92024, .T. ) ;
#80827=LINE ( 'NONE', #27037, #26663 ) ;
#80828=CARTESIAN_POINT ( 'NONE',  ( -8.027368788987615744, 17.96763083595211441, 11.49999999999998934 ) ) ;
#80831=LINE ( 'NONE', #51378, #67407 ) ;
#80834=ORIENTED_EDGE ( 'NONE', *, *, #55978, .T. ) ;
#80835=FACE_OUTER_BOUND ( 'NONE', #80578, .T. ) ;
#80836=CARTESIAN_POINT ( 'NONE',  ( -126.5228709571500616, -23.47593901973090524, -1.443836447538996204 ) ) ;
#80837=CARTESIAN_POINT ( 'NONE',  ( -105.5228709571500758, -23.47593901973090524, -1.443836447538996426 ) ) ;
#80838=DIRECTION ( 'NONE',  ( -1.000000000000000000, -3.773278334444166432E-23, -8.201307841325785021E-29 ) ) ;
#80839=CARTESIAN_POINT ( 'NONE',  ( -80.91152895311172699, -25.20144873054373136, 6.835696071488102099 ) ) ;
#80843=DIRECTION ( 'NONE',  ( 3.773278334444167608E-23, -1.000000000000000000, 0.000000000000000000 ) ) ;
#80844=CARTESIAN_POINT ( 'NONE',  ( 6.088051586893210576, -19.00464151315268424, -1.500000000000002220 ) ) ;
#80846=CARTESIAN_POINT ( 'NONE',  ( -19.08307359429613825, -5.530936995296134917, -1.500000000000002220 ) ) ;
#80847=VERTEX_POINT ( 'NONE', #46858 ) ;
#80848=VECTOR ( 'NONE', #93965, 1000.000000000000114 ) ;
#80849=CARTESIAN_POINT ( 'NONE',  ( -120.5228709571501184, -23.48783264082477373, -1.443836473390081698 ) ) ;
#80852=CARTESIAN_POINT ( 'NONE',  ( 1.081820405348005165, -20.78239343107542680, 11.49999999999999645 ) ) ;
#80854=AXIS2_PLACEMENT_3D ( 'NONE', #49411, #86948, #33160 ) ;
#80856=CARTESIAN_POINT ( 'NONE',  ( 5.898633191892585614, -22.09092271590295198, 11.49999999999999645 ) ) ;
#80857=ORIENTED_EDGE ( 'NONE', *, *, #58941, .T. ) ;
#80858=CARTESIAN_POINT ( 'NONE',  ( -55.22287095715007155, -23.47593901973090169, -1.443836447538997758 ) ) ;
#80859=FACE_OUTER_BOUND ( 'NONE', #74441, .T. ) ;
#80860=VERTEX_POINT ( 'NONE', #83916 ) ;
#80862=CARTESIAN_POINT ( 'NONE',  ( 15.69265952521009488, -12.80212094623039576, 11.49999999999998934 ) ) ;
#80864=FACE_OUTER_BOUND ( 'NONE', #43113, .T. ) ;
#80865=CARTESIAN_POINT ( 'NONE',  ( -100.6228709571500417, -24.92579138211020151, 1.929029949965661572 ) ) ;
#80868=CARTESIAN_POINT ( 'NONE',  ( -79.46841724574004218, -25.31402286304979299, 4.799853472881489225 ) ) ;
#80870=CARTESIAN_POINT ( 'NONE',  ( -17.52916707085001136, 9.785066945116392745, -1.500000000000002220 ) ) ;
#80871=CARTESIAN_POINT ( 'NONE',  ( 7.388015978253313243, 19.69965359013245632, 11.49999999999999645 ) ) ;
#80872=CARTESIAN_POINT ( 'NONE',  ( -29.51986997226218534, -25.07943211551384977, 6.939773859971299252 ) ) ;
#80874=CARTESIAN_POINT ( 'NONE',  ( 20.57837473233041692, -7.934362236255416256, 11.49999999999998934 ) ) ;
#80876=CARTESIAN_POINT ( 'NONE',  ( -39.59566294291796140, -25.27806020191125214, 4.684364630645174721 ) ) ;
#80878=LINE ( 'NONE', #26595, #45202 ) ;
#80881=CARTESIAN_POINT ( 'NONE',  ( -31.52580767185885691, -24.65952944569304250, 1.056160979905695463 ) ) ;
#80882=ORIENTED_EDGE ( 'NONE', *, *, #57250, .F. ) ;
#80883=ORIENTED_EDGE ( 'NONE', *, *, #21166, .T. ) ;
#80886=CARTESIAN_POINT ( 'NONE',  ( -94.62287095715004170, -23.72773821059536559, 11.05748984161097681 ) ) ;
#80887=CARTESIAN_POINT ( 'NONE',  ( 4.502618398017903090, 20.03723546437915104, -1.500000000000002220 ) ) ;
#80888=VERTEX_POINT ( 'NONE', #84415 ) ;
#80891=CARTESIAN_POINT ( 'NONE',  ( -69.52287095715006160, -29.50250786944525672, 11.44777988621623699 ) ) ;
#80892=CARTESIAN_POINT ( 'NONE',  ( -20.55042600948665310, 8.738301046694649798, 11.49999999999998934 ) ) ;
#80894=CARTESIAN_POINT ( 'NONE',  ( -121.9228709571500673, -23.47596703998600631, 11.44779298504227683 ) ) ;
#80895=EDGE_LOOP ( 'NONE', ( #9076, #42873, #16609, #34308 ) ) ;
#80896=CARTESIAN_POINT ( 'NONE',  ( -96.62287095715005592, -23.48783264082478794, -1.443836473390061936 ) ) ;
#80897=CARTESIAN_POINT ( 'NONE',  ( -47.62287095715006302, -23.47596703998600276, 11.44779298504227505 ) ) ;
#80898=CARTESIAN_POINT ( 'NONE',  ( -19.85847575633505713, -6.422239212204448044, 11.49999999999998934 ) ) ;
#80899=ORIENTED_EDGE ( 'NONE', *, *, #49694, .F. ) ;
#80901=VERTEX_POINT ( 'NONE', #77285 ) ;
#80902=ORIENTED_EDGE ( 'NONE', *, *, #80942, .T. ) ;
#80903=CARTESIAN_POINT ( 'NONE',  ( -68.98049337452070517, -25.25935131006976064, 6.552244419545522724 ) ) ;
#80904=CARTESIAN_POINT ( 'NONE',  ( -20.97943885474387216, 2.004451313549292735, -1.500000000000002220 ) ) ;
#80908=CARTESIAN_POINT ( 'NONE',  ( -120.5888102207224790, -24.73531770709095312, 8.716586749053508498 ) ) ;
#80911=PLANE ( 'NONE',  #28752 ) ;
#80912=CARTESIAN_POINT ( 'NONE',  ( -10.61912389536305490, -18.88692380039396213, -1.500000000000002220 ) ) ;
#80913=CARTESIAN_POINT ( 'NONE',  ( -81.22562555205841761, -25.24759741702468219, 6.810744828488381586 ) ) ;
#80914=CARTESIAN_POINT ( 'NONE',  ( 10.43072250204971851, -19.66636941823637841, 11.49999999999999645 ) ) ;
#80915=ORIENTED_EDGE ( 'NONE', *, *, #92398, .T. ) ;
#80916=LINE ( 'NONE', #95645, #35650 ) ;
#80917=CARTESIAN_POINT ( 'NONE',  ( -95.62287095715007013, -23.48786465467241769, 11.44779295918254114 ) ) ;
#80918=FACE_OUTER_BOUND ( 'NONE', #13473, .T. ) ;
#80925=B_SPLINE_CURVE_WITH_KNOTS ( 'NONE', 3,
 ( #22148, #13047, #98278, #92172 ),
 .UNSPECIFIED., .F., .F.,
 ( 4, 4 ),
 ( 0.000000000000000000, 0.0004038461538461851630 ),
 .UNSPECIFIED. ) ;
#80928=CARTESIAN_POINT ( 'NONE',  ( -121.5894513684704208, -24.34968618360934300, 0.1864209137778885528 ) ) ;
#80929=VECTOR ( 'NONE', #38604, 1000.000000000000114 ) ;
#80930=CARTESIAN_POINT ( 'NONE',  ( -48.62287095715009144, -24.34917612406837861, 0.1852690917426599304 ) ) ;
#80931=CARTESIAN_POINT ( 'NONE',  ( -126.5228709571500332, -24.33927499327855770, 9.819080762295802955 ) ) ;
#80933=EDGE_CURVE ( 'NONE', #30322, #82227, #59720, .T. ) ;
#80934=CARTESIAN_POINT ( 'NONE',  ( -130.5728709571500872, -24.94533875906350318, 8.329945116542303296 ) ) ;
#80935=CARTESIAN_POINT ( 'NONE',  ( -15.60622653811170402, 16.18669697583415967, -1.500000000000002220 ) ) ;
#80937=CARTESIAN_POINT ( 'NONE',  ( -96.62287095715005592, -29.50250243563736774, 8.947779886222138046 ) ) ;
#80938=CARTESIAN_POINT ( 'NONE',  ( -101.5506312112252374, -24.35071581493543746, 9.817618358456027039 ) ) ;
#80939=ADVANCED_FACE ( 'NONE', ( #93015 ), #54975, .F. ) ;
#80942=EDGE_CURVE ( 'NONE', #55923, #27877, #37742, .T. ) ;
#80943=CARTESIAN_POINT ( 'NONE',  ( -30.57310351248101554, -25.30557784678703825, 3.856996771331004048 ) ) ;
#80944=CARTESIAN_POINT ( 'NONE',  ( -3.586273028688536257, -19.27814873881845514, -1.500000000000002220 ) ) ;
#80946=CARTESIAN_POINT ( 'NONE',  ( -49.54372330632813259, -25.28866772429660870, 4.191984911758548371 ) ) ;
#80948=CARTESIAN_POINT ( 'NONE',  ( 8.792760106793807040, 19.66521392739144858, 11.49999999999998934 ) ) ;
#80951=CARTESIAN_POINT ( 'NONE',  ( -80.76567584835706270, -25.30394766154488551, 4.998963552913667563 ) ) ;
#80952=CARTESIAN_POINT ( 'NONE',  ( -63.58953762381672448, -24.66019654487198665, 8.947790411086129936 ) ) ;
#80953=FACE_OUTER_BOUND ( 'NONE', #89145, .T. ) ;
#80954=CARTESIAN_POINT ( 'NONE',  ( -14.90462150274475306, 17.49973755783957685, -1.500000000000002220 ) ) ;
#80956=CARTESIAN_POINT ( 'NONE',  ( -102.6228709571500559, -23.47596703998600631, 11.44779298504227683 ) ) ;
#80958=CARTESIAN_POINT ( 'NONE',  ( -16.72505113720834657, 11.10480813184383742, 11.49999999999999645 ) ) ;
#80959=CARTESIAN_POINT ( 'NONE',  ( -110.2646033073992129, -25.28814069144094034, 2.833559589122900846 ) ) ;
#80960=FACE_OUTER_BOUND ( 'NONE', #87501, .T. ) ;
#80961=DIRECTION ( 'NONE',  ( -3.773278334453079618E-23, 0.9999999999976377785, 2.173523156925979975E-06 ) ) ;
#80962=CARTESIAN_POINT ( 'NONE',  ( -65.62287095715005592, -23.47593901973091235, -1.443836447539006196 ) ) ;
#80963=EDGE_CURVE ( 'NONE', #76269, #99833, #13679, .T. ) ;
#80965=CARTESIAN_POINT ( 'NONE',  ( 15.03354914759215966, -12.96403794047452607, 11.49999999999998934 ) ) ;
#80966=DIRECTION ( 'NONE',  ( -3.773278334453079030E-23, 0.9999999999976377785, 2.173523156925979128E-06 ) ) ;
#80967=CARTESIAN_POINT ( 'NONE',  ( 12.09797951242163805, 15.59582292391970704, -1.500000000000002220 ) ) ;
#80968=CARTESIAN_POINT ( 'NONE',  ( -42.51346541940907287, -23.73766607897670156, -1.055555164236442689 ) ) ;
#80970=CARTESIAN_POINT ( 'NONE',  ( -115.6228709571500559, -24.99132157543166954, 2.256160258750667502 ) ) ;
#80971=CARTESIAN_POINT ( 'NONE',  ( -79.52287095715003318, -23.95044443724990657, 10.65354141964648704 ) ) ;
#80972=CARTESIAN_POINT ( 'NONE',  ( -20.60669311552257810, 0.8253496925510150906, 11.49999999999999645 ) ) ;
#80975=CARTESIAN_POINT ( 'NONE',  ( -18.78231125015805958, 12.62931641965373153, 11.49999999999999645 ) ) ;
#80977=PLANE ( 'NONE',  #41080 ) ;
#80978=CARTESIAN_POINT ( 'NONE',  ( -97.59370113735080565, -23.96119346886881374, -0.6495511937832058047 ) ) ;
#80980=B_SPLINE_CURVE_WITH_KNOTS ( 'NONE', 3,
 ( #51056, #51556, #75367, #74868, #67283, #38304 ),
 .UNSPECIFIED., .F., .F.,
 ( 4, 2, 4 ),
 ( 0.000000000000000000, 0.001380764517854764749, 0.002761529035709529498 ),
 .UNSPECIFIED. ) ;
#80981=EDGE_CURVE ( 'NONE', #89617, #20503, #677, .T. ) ;
#80982=CARTESIAN_POINT ( 'NONE',  ( -110.2093792378191921, -25.29160350784524880, 5.585409231008217290 ) ) ;
#80983=CARTESIAN_POINT ( 'NONE',  ( -45.55620429048339304, -25.00158670708908915, 2.256160236439166855 ) ) ;
#80987=ORIENTED_EDGE ( 'NONE', *, *, #65294, .T. ) ;
#80988=FACE_OUTER_BOUND ( 'NONE', #18412, .T. ) ;
#80989=CARTESIAN_POINT ( 'NONE',  ( -11.09240565882118368, -20.00103931635436538, -1.500000000000002220 ) ) ;
#80990=CARTESIAN_POINT ( 'NONE',  ( -110.3346797185884327, -25.18492896333868813, 3.293943116708551777 ) ) ;
#80991=AXIS2_PLACEMENT_3D ( 'NONE', #35593, #96980, #80764 ) ;
#80992=DIRECTION ( 'NONE',  ( -3.773278334453079030E-23, 0.9999999999976377785, 2.173523156925978705E-06 ) ) ;
#80993=CARTESIAN_POINT ( 'NONE',  ( -32.62287095715004881, -23.48783264082477729, -1.443836473390074371 ) ) ;
#80994=CARTESIAN_POINT ( 'NONE',  ( -21.16606679798846358, 7.723709098063864076, 11.49999999999999645 ) ) ;
#80995=EDGE_LOOP ( 'NONE', ( #32424, #95982, #74766, #92079 ) ) ;
#80996=CARTESIAN_POINT ( 'NONE',  ( -43.48728809283164765, -24.51314013834316086, 0.6176544820404143987 ) ) ;
#80997=CARTESIAN_POINT ( 'NONE',  ( -1.948345350117603125, -21.87844622001750139, 11.49999999999998934 ) ) ;
#80999=CARTESIAN_POINT ( 'NONE',  ( -111.5135334585156102, -24.65952944569305316, 1.056160979905705677 ) ) ;
#81000=CARTESIAN_POINT ( 'NONE',  ( -112.6228709571500559, -24.64965695001469115, 8.947790433994176951 ) ) ;
#81001=VERTEX_POINT ( 'NONE', #94525 ) ;
#81002=CARTESIAN_POINT ( 'NONE',  ( -35.62287095715005592, -29.50250786944525672, 11.44777988621624232 ) ) ;
#81003=ADVANCED_FACE ( 'NONE', ( #49879 ), #2199, .F. ) ;
#81004=DIRECTION ( 'NONE',  ( -3.773278334453079618E-23, 0.9999999999976377785, 2.173523156925979975E-06 ) ) ;
#81005=ORIENTED_EDGE ( 'NONE', *, *, #23758, .T. ) ;
#81006=LINE ( 'NONE', #51062, #61513 ) ;
#81007=CARTESIAN_POINT ( 'NONE',  ( -14.05295919346176170, -14.94737400546395456, 11.49999999999998934 ) ) ;
#81009=B_SPLINE_CURVE_WITH_KNOTS ( 'NONE', 3,
 ( #84722, #14706, #76099, #90340 ),
 .UNSPECIFIED., .F., .F.,
 ( 4, 4 ),
 ( 1.387778780781445676E-17, 0.0001000000000000028508 ),
 .UNSPECIFIED. ) ;
#81012=CARTESIAN_POINT ( 'NONE',  ( -126.5228709571500332, -24.33832256527048088, 0.1851278514138670062 ) ) ;
#81013=CARTESIAN_POINT ( 'NONE',  ( -5.338719972479099241, 22.46511350730333589, 11.49999999999998934 ) ) ;
#81014=CARTESIAN_POINT ( 'NONE',  ( -104.5480580092806804, -24.66019654487200441, 8.947790411086108620 ) ) ;
#81015=CARTESIAN_POINT ( 'NONE',  ( 15.61528876134825161, -13.05345633644532732, -1.500000000000002220 ) ) ;
#81016=ADVANCED_FACE ( 'NONE', ( #25008 ), #32124, .F. ) ;
#81017=ORIENTED_EDGE ( 'NONE', *, *, #8865, .T. ) ;
#81019=CARTESIAN_POINT ( 'NONE',  ( -29.62069581956789222, -23.40858285148628681, 11.44779303447556984 ) ) ;
#81020=CARTESIAN_POINT ( 'NONE',  ( -105.5132832374360277, -24.40034930558991633, 0.3402023900116059041 ) ) ;
#81021=CARTESIAN_POINT ( 'NONE',  ( -35.55620429048339304, -23.47593901973091235, -1.443836447539011525 ) ) ;
#81023=B_SPLINE_CURVE_WITH_KNOTS ( 'NONE', 3,
 ( #66643, #20922, #1851, #25678, #64778, #56147 ),
 .UNSPECIFIED., .F., .F.,
 ( 4, 2, 4 ),
 ( 1.570887131794638196E-05, 0.001396322306279762157, 0.002776935741241578007 ),
 .UNSPECIFIED. ) ;
#81024=CARTESIAN_POINT ( 'NONE',  ( -29.24577077129365321, -24.76881379442145814, 4.691559412919051653 ) ) ;
#81025=PLANE ( 'NONE',  #97758 ) ;
#81026=ORIENTED_EDGE ( 'NONE', *, *, #34721, .F. ) ;
#81027=B_SPLINE_CURVE_WITH_KNOTS ( 'NONE', 3,
 ( #34984, #13624, #28868, #65962, #59830, #90764 ),
 .UNSPECIFIED., .F., .F.,
 ( 4, 2, 4 ),
 ( 0.000000000000000000, 0.001380764517853249034, 0.002761529035706497635 ),
 .UNSPECIFIED. ) ;
#81028=CARTESIAN_POINT ( 'NONE',  ( -7.357705842588929457, 19.43699106120834230, 11.49999999999998934 ) ) ;
#81029=ORIENTED_EDGE ( 'NONE', *, *, #2639, .F. ) ;
#81031=CARTESIAN_POINT ( 'NONE',  ( -101.5603755832771071, -23.48783264082477373, -1.443836473390089248 ) ) ;
#81034=CARTESIAN_POINT ( 'NONE',  ( -51.16340783650578317, -25.30574378417172454, 5.002672300970606223 ) ) ;
#81036=ORIENTED_EDGE ( 'NONE', *, *, #19293, .T. ) ;
#81037=CARTESIAN_POINT ( 'NONE',  ( -88.55620429048339304, -24.65952944569304606, 1.056160979905699904 ) ) ;
#81038=DIRECTION ( 'NONE',  ( -3.773278334453079618E-23, 0.9999999999976377785, 2.173523156925979975E-06 ) ) ;
#81039=CARTESIAN_POINT ( 'NONE',  ( -74.62287095715002749, -24.33832256527048088, 0.1851278514138608444 ) ) ;
#81040=CARTESIAN_POINT ( 'NONE',  ( -13.14421341422731260, -17.72855101262432242, 11.49999999999999645 ) ) ;
#81043=CARTESIAN_POINT ( 'NONE',  ( -11.86362535333686807, -19.25999739251378173, 11.49999999999998934 ) ) ;
#81044=CARTESIAN_POINT ( 'NONE',  ( -115.5505208059758360, -24.92592662359561473, 8.075495903017996469 ) ) ;
#81045=VERTEX_POINT ( 'NONE', #10798 ) ;
#81047=PLANE ( 'NONE',  #98473 ) ;
#81048=VECTOR ( 'NONE', #15847, 1000.000000000000114 ) ;
#81049=CARTESIAN_POINT ( 'NONE',  ( -128.5562042904833788, -23.48783264082479150, -1.443836473390056829 ) ) ;
#81050=EDGE_LOOP ( 'NONE', ( #80834, #10482, #75674, #6624 ) ) ;
#81051=CARTESIAN_POINT ( 'NONE',  ( -18.51692787870624102, -10.26217664800131502, 11.49999999999998934 ) ) ;
#81055=CARTESIAN_POINT ( 'NONE',  ( 21.78807519107708401, 4.755904613692067073, -1.500000000000002220 ) ) ;
#81057=ADVANCED_FACE ( 'NONE', ( #94024 ), #79798, .F. ) ;
#81058=ORIENTED_EDGE ( 'NONE', *, *, #96169, .T. ) ;
#81061=CARTESIAN_POINT ( 'NONE',  ( -91.52287095715006160, -29.50250243563736774, 8.947779886222139822 ) ) ;
#81062=B_SPLINE_CURVE_WITH_KNOTS ( 'NONE', 3,
 ( #1737, #88474, #56034, #18948 ),
 .UNSPECIFIED., .F., .F.,
 ( 4, 4 ),
 ( 0.5891933397657490579, 0.5901940868065144175 ),
 .UNSPECIFIED. ) ;
#81063=CARTESIAN_POINT ( 'NONE',  ( -36.49041699993523480, -24.35071581493542325, 9.817618358456030592 ) ) ;
#81066=CARTESIAN_POINT ( 'NONE',  ( 2.628080361126900133, -19.32819128710564272, 11.49999999999998934 ) ) ;
#81068=VECTOR ( 'NONE', #6360, 1000.000000000000114 ) ;
#81069=CARTESIAN_POINT ( 'NONE',  ( -2.751442626040462081, 21.25944542233241563, 11.49999999999998934 ) ) ;
#81073=PLANE ( 'NONE',  #6891 ) ;
#81074=CARTESIAN_POINT ( 'NONE',  ( -22.16177213047534877, -5.259615592301647879, -1.500000000000002220 ) ) ;
#81075=AXIS2_PLACEMENT_3D ( 'NONE', #82678, #11179, #97894 ) ;
#81076=CARTESIAN_POINT ( 'NONE',  ( -98.51142843485534684, -24.34968618360934300, 0.1864209137778828629 ) ) ;
#81078=CARTESIAN_POINT ( 'NONE',  ( -7.573260116017839216, 18.43532004384545786, 11.49999999999999645 ) ) ;
#81080=CARTESIAN_POINT ( 'NONE',  ( -39.48048556723951208, -24.66019654487198665, 8.947790411086131712 ) ) ;
#81081=CARTESIAN_POINT ( 'NONE',  ( -81.62287095715005592, -29.50248528299804818, 1.056150453629038477 ) ) ;
#81082=VERTEX_POINT ( 'NONE', #87924 ) ;
#81084=PLANE ( 'NONE',  #88234 ) ;
#81085=CARTESIAN_POINT ( 'NONE',  ( -32.99702443869961854, -25.31600595412499644, 6.101236642668423471 ) ) ;
#81086=CARTESIAN_POINT ( 'NONE',  ( 16.98214085172422827, 13.50221961261776293, 11.49999999999998934 ) ) ;
#81087=CARTESIAN_POINT ( 'NONE',  ( -56.59864015429606354, -23.96169478059713498, 10.65365249895718236 ) ) ;
#81088=CARTESIAN_POINT ( 'NONE',  ( 15.80261042061247068, 11.49252619723154112, -1.500000000000002220 ) ) ;
#81091=FACE_OUTER_BOUND ( 'NONE', #65659, .T. ) ;
#81092=CARTESIAN_POINT ( 'NONE',  ( 13.31029742451639386, -15.53102932315203510, 11.49999999999999645 ) ) ;
#81094=CARTESIAN_POINT ( 'NONE',  ( -118.6228709571500559, -23.73907113216991860, -1.053371485793222151 ) ) ;
#81095=ORIENTED_EDGE ( 'NONE', *, *, #36786, .T. ) ;
#81097=CARTESIAN_POINT ( 'NONE',  ( -39.51912653461286595, -25.28892541655923054, 3.844034288105113273 ) ) ;
#81098=DIRECTION ( 'NONE',  ( 0.000000000000000000, -2.173523156925979552E-06, 0.9999999999976378895 ) ) ;
#81099=CARTESIAN_POINT ( 'NONE',  ( -49.27881313098881577, -25.25138871933836171, 6.114505553594992371 ) ) ;
#81100=CARTESIAN_POINT ( 'NONE',  ( -31.24388727629347784, -24.87479601683088148, 8.247789944647559324 ) ) ;
#81102=CARTESIAN_POINT ( 'NONE',  ( -111.3776484685884469, -25.29712067403330877, 4.332404411321261861 ) ) ;
#81103=ADVANCED_FACE ( 'NONE', ( #3204 ), #72206, .T. ) ;
#81104=CARTESIAN_POINT ( 'NONE',  ( 8.869223403490039459, -21.23658630136709391, 11.49999999999999645 ) ) ;
#81105=CARTESIAN_POINT ( 'NONE',  ( 22.50852769316577096, -3.342225187595919689, 11.49999999999998934 ) ) ;
#81106=CARTESIAN_POINT ( 'NONE',  ( -70.95923861438973290, -25.07168450528815740, 7.426717504460598640 ) ) ;
#81107=CARTESIAN_POINT ( 'NONE',  ( -94.22287095715012128, -23.47593901973090880, -1.443836447538997314 ) ) ;
#81108=CARTESIAN_POINT ( 'NONE',  ( -90.54767163586556933, -24.52300882791529801, 0.6510814631126391472 ) ) ;
#81110=FACE_OUTER_BOUND ( 'NONE', #21696, .T. ) ;
#81112=CARTESIAN_POINT ( 'NONE',  ( -1.678574117887026373, -21.80011532881206548, 11.49999999999998934 ) ) ;
#81114=CARTESIAN_POINT ( 'NONE',  ( -70.55620429048337883, -24.99132157543166954, 2.256160258750667946 ) ) ;
#81115=LINE ( 'NONE', #13588, #23342 ) ;
#81118=ORIENTED_EDGE ( 'NONE', *, *, #78908, .F. ) ;
#81119=CARTESIAN_POINT ( 'NONE',  ( 0.5039804632396667206, -20.40334623801319580, -1.500000000000002220 ) ) ;
#81121=ORIENTED_EDGE ( 'NONE', *, *, #71265, .T. ) ;
#81122=VERTEX_POINT ( 'NONE', #49376 ) ;
#81123=ORIENTED_EDGE ( 'NONE', *, *, #978, .F. ) ;
#81124=CARTESIAN_POINT ( 'NONE',  ( -20.90396053131702914, -9.656267258341529214, 11.49999999999998934 ) ) ;
#81126=CARTESIAN_POINT ( 'NONE',  ( 15.73562052650688514, -12.66937975264744587, -1.500000000000002220 ) ) ;
#81127=EDGE_LOOP ( 'NONE', ( #28834, #70381, #99612, #87538 ) ) ;
#81128=FACE_OUTER_BOUND ( 'NONE', #84902, .T. ) ;
#81129=CARTESIAN_POINT ( 'NONE',  ( -48.52287095715005449, -24.35013146730203815, 9.818937971375097717 ) ) ;
#81130=B_SPLINE_CURVE_WITH_KNOTS ( 'NONE', 3,
 ( #10556, #26285, #72469, #19657 ),
 .UNSPECIFIED., .F., .F.,
 ( 4, 4 ),
 ( 0.2699787096657541574, 0.2789851409378695801 ),
 .UNSPECIFIED. ) ;
#81131=AXIS2_PLACEMENT_3D ( 'NONE', #61980, #70082, #15281 ) ;
#81132=CARTESIAN_POINT ( 'NONE',  ( -95.58289945215418015, -25.00158670708911046, 2.256160236439221034 ) ) ;
#81133=CARTESIAN_POINT ( 'NONE',  ( -123.5562042904833788, -23.47593901973091235, -1.443836447538997536 ) ) ;
#81134=CARTESIAN_POINT ( 'NONE',  ( 21.34331307443176584, 0.5271963136488534429, 11.49999999999999645 ) ) ;
#81135=VERTEX_POINT ( 'NONE', #48366 ) ;
#81139=CARTESIAN_POINT ( 'NONE',  ( 21.27325221474336914, 6.521069146585026566, 11.49999999999998934 ) ) ;
#81140=CARTESIAN_POINT ( 'NONE',  ( -18.79711486612840332, 8.613068827758688428, -1.500000000000002220 ) ) ;
#81145=CARTESIAN_POINT ( 'NONE',  ( -68.92380496721939664, -25.20650855361216713, 6.812664954086296909 ) ) ;
#81148=VERTEX_POINT ( 'NONE', #71199 ) ;
#81150=CARTESIAN_POINT ( 'NONE',  ( 5.581485548573628996, 20.18083795961418403, -1.500000000000002220 ) ) ;
#81151=CARTESIAN_POINT ( 'NONE',  ( -21.09739860443290382, 5.981408608369527258, 11.49999999999999645 ) ) ;
#81153=CARTESIAN_POINT ( 'NONE',  ( -18.84819291449097278, 12.34854029719970825, 11.49999999999998934 ) ) ;
#81155=CARTESIAN_POINT ( 'NONE',  ( 13.87900837158347755, -15.70065903812341013, 11.49999999999998934 ) ) ;
#81156=CARTESIAN_POINT ( 'NONE',  ( -26.09849696787948403, -24.88148762671936964, 5.165052607479680979 ) ) ;
#81158=CARTESIAN_POINT ( 'NONE',  ( -119.5178257542950035, -24.51419770103158768, 9.386484678747164523 ) ) ;
#81159=CARTESIAN_POINT ( 'NONE',  ( -68.52287095715007581, -23.47593901973090524, -1.443836447538997092 ) ) ;
#81160=ORIENTED_EDGE ( 'NONE', *, *, #28265, .F. ) ;
#81162=ORIENTED_EDGE ( 'NONE', *, *, #29886, .F. ) ;
#81163=CARTESIAN_POINT ( 'NONE',  ( -52.62810917408141620, -24.51314013834315375, 0.6176544820404124003 ) ) ;
#81165=CARTESIAN_POINT ( 'NONE',  ( 19.88731969966643476, 8.162773808193900749, -1.500000000000002220 ) ) ;
#81166=CARTESIAN_POINT ( 'NONE',  ( -26.16566273216211513, -24.93396852503405370, 5.877190228123938986 ) ) ;
#81167=CARTESIAN_POINT ( 'NONE',  ( 20.91448408463407205, 2.778442817847782020, 11.49999999999998934 ) ) ;
#81168=CARTESIAN_POINT ( 'NONE',  ( -99.66789520314513595, -25.23538937966463891, 3.604794963105668160 ) ) ;
#81170=CARTESIAN_POINT ( 'NONE',  ( -96.62287095715005592, -23.47596703998600631, 11.44779298504227860 ) ) ;
#81171=CARTESIAN_POINT ( 'NONE',  ( -81.52287095715001897, -24.66019654487199375, 8.947790411086126383 ) ) ;
#81172=CARTESIAN_POINT ( 'NONE',  ( -129.6238143503192077, -23.73791477778912906, 11.05961554403170233 ) ) ;
#81173=B_SPLINE_CURVE_WITH_KNOTS ( 'NONE', 3,
 ( #5646, #98483, #93761, #13252, #59446, #83270, #44717, #37097, #59955, #5154, #90884, #16633, #51836, #28983, #52332, #39483 ),
 .UNSPECIFIED., .F., .F.,
 ( 4, 2, 2, 2, 2, 2, 2, 4 ),
 ( 8.673617379884035472E-19, 0.0004698675029436834511, 0.0007048012544155247971, 0.0009397350058873660348, 0.001174668757359207272, 0.001409602508831048727, 0.001644536260302889965, 0.001879470011774731202 ),
 .UNSPECIFIED. ) ;
#81174=CARTESIAN_POINT ( 'NONE',  ( 16.78392297789021015, 14.29496084597832883, -1.500000000000002220 ) ) ;
#81176=B_SPLINE_CURVE_WITH_KNOTS ( 'NONE', 3,
 ( #9006, #70920, #1410, #32344, #63320, #94238 ),
 .UNSPECIFIED., .F., .F.,
 ( 4, 2, 4 ),
 ( 0.000000000000000000, 0.001380764517853252287, 0.002761529035706504574 ),
 .UNSPECIFIED. ) ;
#81177=CARTESIAN_POINT ( 'NONE',  ( -65.52204159167497721, -23.48786465467241058, 11.44779295918254824 ) ) ;
#81178=EDGE_CURVE ( 'NONE', #79014, #98210, #65610, .T. ) ;
#81179=LINE ( 'NONE', #42635, #57909 ) ;
#81180=CARTESIAN_POINT ( 'NONE',  ( -41.64605464260454681, -25.31624614353306058, 4.957686406151942116 ) ) ;
#81181=CARTESIAN_POINT ( 'NONE',  ( -47.52287095715007581, -23.47593901973090169, -1.443836447538997092 ) ) ;
#81182=CARTESIAN_POINT ( 'NONE',  ( -32.52287095715006160, -24.64898659630528854, 1.056161002820817485 ) ) ;
#81183=CARTESIAN_POINT ( 'NONE',  ( -6.767052838139933080, -20.26514109264706676, 11.49999999999998934 ) ) ;
#81184=CARTESIAN_POINT ( 'NONE',  ( -97.62287095715005592, -23.48786465467241058, 11.44779295918254114 ) ) ;
#81185=CARTESIAN_POINT ( 'NONE',  ( -48.85382640980453317, -25.31392319263090585, 5.203681702801227438 ) ) ;
#81187=EDGE_CURVE ( 'NONE', #89111, #39193, #83957, .T. ) ;
#81189=CARTESIAN_POINT ( 'NONE',  ( -80.54762525791510086, -25.12326838703506127, 7.100031122939245876 ) ) ;
#81190=CARTESIAN_POINT ( 'NONE',  ( 21.78986343443989071, 5.811249688775594002, -1.500000000000002220 ) ) ;
#81191=ADVANCED_FACE ( 'NONE', ( #12279 ), #43256, .T. ) ;
#81192=CARTESIAN_POINT ( 'NONE',  ( -49.27764846858840997, -29.50249634415583699, 6.145195751613371726 ) ) ;
#81195=CARTESIAN_POINT ( 'NONE',  ( -79.60030546162484200, -23.73766607897669800, -1.055555164236459564 ) ) ;
#81196=CARTESIAN_POINT ( 'NONE',  ( 17.76913753361954562, 8.601950719843506121, 11.49999999999999645 ) ) ;
#81198=CARTESIAN_POINT ( 'NONE',  ( -67.58021307568701275, -24.65952944569304961, 1.056160979905700570 ) ) ;
#81199=ORIENTED_EDGE ( 'NONE', *, *, #92120, .T. ) ;
#81200=ADVANCED_FACE ( 'NONE', ( #58978 ), #11295, .T. ) ;
#81201=DIRECTION ( 'NONE',  ( -3.773278334453080206E-23, 0.9999999999976377785, 2.173523156925979975E-06 ) ) ;
#81202=FACE_OUTER_BOUND ( 'NONE', #98753, .T. ) ;
#81203=CARTESIAN_POINT ( 'NONE',  ( -101.1692196971220312, -25.12268517087270325, 6.877671137330668039 ) ) ;
#81204=CARTESIAN_POINT ( 'NONE',  ( -19.28869470675124731, 9.786980993800005635, -1.500000000000002220 ) ) ;
#81206=CARTESIAN_POINT ( 'NONE',  ( -19.23900614489824079, 2.250179475969715348, -1.500000000000002220 ) ) ;
#81207=ADVANCED_FACE ( 'NONE', ( #43748 ), #40265, .T. ) ;
#81209=CARTESIAN_POINT ( 'NONE',  ( -85.62287095715002749, -25.00182538069145011, 7.747789668545099317 ) ) ;
#81210=CARTESIAN_POINT ( 'NONE',  ( -12.15653940608521566, -15.58205587995076868, 11.49999999999998934 ) ) ;
#81212=B_SPLINE_CURVE_WITH_KNOTS ( 'NONE', 3,
 ( #2079, #33513, #19275, #17284 ),
 .UNSPECIFIED., .F., .F.,
 ( 4, 4 ),
 ( 0.000000000000000000, 9.999999999998897304E-05 ),
 .UNSPECIFIED. ) ;
#81214=CARTESIAN_POINT ( 'NONE',  ( -2.356373108420451334, 20.14613781377289214, 11.49999999999999645 ) ) ;
#81216=B_SPLINE_CURVE_WITH_KNOTS ( 'NONE', 3,
 ( #64198, #29094, #21966, #82386 ),
 .UNSPECIFIED., .F., .F.,
 ( 4, 4 ),
 ( 0.000000000000000000, 0.0001000000000000028644 ),
 .UNSPECIFIED. ) ;
#81217=B_SPLINE_CURVE_WITH_KNOTS ( 'NONE', 3,
 ( #19904, #20900, #27539, #4699, #67111, #65622, #82311, #58496, #67602, #96539 ),
 .UNSPECIFIED., .F., .F.,
 ( 4, 2, 2, 2, 4 ),
 ( 1.844036349440735311E-17, 0.0001572768558401152516, 0.0003145537116802120717, 0.0004718305675203088648, 0.0006291074233604057120 ),
 .UNSPECIFIED. ) ;
#81219=CARTESIAN_POINT ( 'NONE',  ( -99.54045094251550552, -25.27399224497114005, 4.126029246454620214 ) ) ;
#81220=LINE ( 'NONE', #28417, #50961 ) ;
#81224=CARTESIAN_POINT ( 'NONE',  ( 12.62869658624171976, -15.57725692549414376, -1.500000000000002220 ) ) ;
#81225=CARTESIAN_POINT ( 'NONE',  ( -51.55620429048339304, -23.47596703998600276, 11.44779298504227505 ) ) ;
#81226=ORIENTED_EDGE ( 'NONE', *, *, #92274, .T. ) ;
#81228=CARTESIAN_POINT ( 'NONE',  ( -90.55620429048339304, -23.47596703998600631, 11.44779298504227683 ) ) ;
#81231=DIRECTION ( 'NONE',  ( -3.773278334453079030E-23, 0.9999999999976377785, 2.173523156925979128E-06 ) ) ;
#81232=CARTESIAN_POINT ( 'NONE',  ( -73.54978490721288154, -24.15543982623907127, -0.2315651400026654816 ) ) ;
#81236=ORIENTED_EDGE ( 'NONE', *, *, #36844, .T. ) ;
#81237=CARTESIAN_POINT ( 'NONE',  ( 18.91379238805564356, 7.493326543281090935, -1.500000000000002220 ) ) ;
#81238=ORIENTED_EDGE ( 'NONE', *, *, #59749, .T. ) ;
#81239=CARTESIAN_POINT ( 'NONE',  ( -14.16064136294604303, -18.02537036913223290, -1.500000000000002220 ) ) ;
#81242=CARTESIAN_POINT ( 'NONE',  ( -49.10646091633891075, -25.26830347608276028, 4.049788970800419996 ) ) ;
#81243=CARTESIAN_POINT ( 'NONE',  ( -76.52287095715006160, -24.33832256527049154, 0.1851278514138614828 ) ) ;
#81244=CARTESIAN_POINT ( 'NONE',  ( -74.58953762381673869, -23.47593901973091235, -1.443836447539006196 ) ) ;
#81245=CARTESIAN_POINT ( 'NONE',  ( 9.480266252741309074, -18.97159823121752709, 11.49999999999999645 ) ) ;
#81246=CARTESIAN_POINT ( 'NONE',  ( -21.14524153552446606, 6.695245452574716261, -1.500000000000002220 ) ) ;
#81248=CARTESIAN_POINT ( 'NONE',  ( 4.697267095454844998, -20.06606415395816967, 11.49999999999998934 ) ) ;
#81249=EDGE_CURVE ( 'NONE', #30827, #53562, #81453, .T. ) ;
#81251=CARTESIAN_POINT ( 'NONE',  ( -41.64113970441989920, -24.15543982623907127, -0.2315651400026566831 ) ) ;
#81253=FACE_OUTER_BOUND ( 'NONE', #80327, .T. ) ;
#81254=CARTESIAN_POINT ( 'NONE',  ( -77.52287095715010423, -23.47593901973090524, -1.443836447538997092 ) ) ;
#81255=VERTEX_POINT ( 'NONE', #61971 ) ;
#81257=VERTEX_POINT ( 'NONE', #22871 ) ;
#81259=CARTESIAN_POINT ( 'NONE',  ( -28.59442033382131854, -23.99963963181664539, 10.23563545308467049 ) ) ;
#81261=CARTESIAN_POINT ( 'NONE',  ( 13.57807927624399902, 15.74560944506941951, -1.500000000000002220 ) ) ;
#81262=CARTESIAN_POINT ( 'NONE',  ( 12.82194709444435077, -17.51738216156474337, 11.49999999999999645 ) ) ;
#81263=ORIENTED_EDGE ( 'NONE', *, *, #76568, .T. ) ;
#81266=CARTESIAN_POINT ( 'NONE',  ( -122.5228709571500616, -24.64898659630368272, 1.056161002820833028 ) ) ;
#81267=CARTESIAN_POINT ( 'NONE',  ( 17.77913403553526805, 13.70458096452923691, -1.500000000000002220 ) ) ;
#81273=CARTESIAN_POINT ( 'NONE',  ( -98.52287095715007581, -24.33927499327855415, 9.819080762295810061 ) ) ;
#81275=CARTESIAN_POINT ( 'NONE',  ( -129.5228709571500758, -24.64898659630529920, 1.056161002820834804 ) ) ;
#81277=EDGE_CURVE ( 'NONE', #84725, #73156, #14771, .T. ) ;
#81279=ORIENTED_EDGE ( 'NONE', *, *, #72243, .F. ) ;
#81281=VERTEX_POINT ( 'NONE', #44746 ) ;
#81282=CARTESIAN_POINT ( 'NONE',  ( 13.65650298889772962, 16.33668418983593185, -1.500000000000002220 ) ) ;
#81284=CARTESIAN_POINT ( 'NONE',  ( -100.7110842131079522, -25.12685321106879144, 7.079481877294677261 ) ) ;
#81285=CARTESIAN_POINT ( 'NONE',  ( 21.83365961380331655, 0.8745889840297637052, -1.500000000000002220 ) ) ;
#81286=CARTESIAN_POINT ( 'NONE',  ( -45.62287095715004881, -23.48783264082478084, -1.443836473390070374 ) ) ;
#81287=CARTESIAN_POINT ( 'NONE',  ( 2.978076788109338402, -22.46882643481310282, 11.49999999999998934 ) ) ;
#81288=CARTESIAN_POINT ( 'NONE',  ( -41.17181748269097596, -25.18430928094562660, 3.555109957723386671 ) ) ;
#81290=CARTESIAN_POINT ( 'NONE',  ( -19.20277006422315225, 10.48866939257135833, -1.500000000000002220 ) ) ;
#81292=EDGE_LOOP ( 'NONE', ( #71534, #19372, #18623, #80163 ) ) ;
#81294=CARTESIAN_POINT ( 'NONE',  ( -126.5228709571500616, -24.65952944569305316, 1.056160979905707675 ) ) ;
#81295=EDGE_CURVE ( 'NONE', #13356, #54341, #10100, .T. ) ;
#81296=EDGE_CURVE ( 'NONE', #50699, #39987, #23370, .T. ) ;
#81297=EDGE_LOOP ( 'NONE', ( #49738, #21706, #35775, #14110 ) ) ;
#81298=CARTESIAN_POINT ( 'NONE',  ( -30.58447015329645069, -25.11083922187778583, 7.243003598645814556 ) ) ;
#81301=CARTESIAN_POINT ( 'NONE',  ( -0.04484292967123595236, -22.46947303600939705, 1.633150109380534509 ) ) ;
#81302=CARTESIAN_POINT ( 'NONE',  ( 13.48273455363431772, -16.43370779934446801, 11.49999999999998934 ) ) ;
#81303=DIRECTION ( 'NONE',  ( 3.773278334444166432E-23, -1.000000000000000000, 0.000000000000000000 ) ) ;
#81304=CARTESIAN_POINT ( 'NONE',  ( -26.48766330312332684, -24.97064563520116920, 3.017960392606179543 ) ) ;
#81305=B_SPLINE_CURVE_WITH_KNOTS ( 'NONE', 3,
 ( #81656, #95873, #17754, #80654, #80154, #12127 ),
 .UNSPECIFIED., .F., .F.,
 ( 4, 2, 4 ),
 ( 1.570887131794952276E-05, 0.001396322306279763675, 0.002776935741241577573 ),
 .UNSPECIFIED. ) ;
#81306=ADVANCED_FACE ( 'NONE', ( #15274 ), #60973, .T. ) ;
#81307=CARTESIAN_POINT ( 'NONE',  ( -85.56476876785632157, -23.48783264082476308, -1.443836473390098796 ) ) ;
#81308=CARTESIAN_POINT ( 'NONE',  ( -68.60258773187044312, -23.73766607897669445, -1.055555164236457788 ) ) ;
#81310=CARTESIAN_POINT ( 'NONE',  ( -117.5545740405765684, -24.15620529776629510, 10.23563542870659582 ) ) ;
#81312=CARTESIAN_POINT ( 'NONE',  ( -19.37596289572233488, 2.755671585415585767, 11.49999999999999645 ) ) ;
#81313=CARTESIAN_POINT ( 'NONE',  ( -95.55620429048337883, -23.48783264082478439, -1.443836473390061492 ) ) ;
#81314=CARTESIAN_POINT ( 'NONE',  ( -28.07520560075130334, -24.67782888724788748, 8.218989154575222500 ) ) ;
#81316=EDGE_CURVE ( 'NONE', #21767, #3088, #77167, .T. ) ;
#81317=CARTESIAN_POINT ( 'NONE',  ( -46.62287095715004881, -29.50248528299804818, 1.056150453629033370 ) ) ;
#81321=CARTESIAN_POINT ( 'NONE',  ( -81.52676753278062449, -25.24813894920551505, 7.119670133019518232 ) ) ;
#81322=CARTESIAN_POINT ( 'NONE',  ( 15.15379598424239838, -12.58889634127381640, -1.500000000000002220 ) ) ;
#81323=EDGE_CURVE ( 'NONE', #67443, #60922, #22121, .T. ) ;
#81324=ORIENTED_EDGE ( 'NONE', *, *, #99352, .F. ) ;
#81325=B_SPLINE_CURVE_WITH_KNOTS ( 'NONE', 3,
 ( #96312, #11075, #34914, #41532 ),
 .UNSPECIFIED., .F., .F.,
 ( 4, 4 ),
 ( 0.000000000000000000, 0.0001000000000000028644 ),
 .UNSPECIFIED. ) ;
#81333=CARTESIAN_POINT ( 'NONE',  ( -103.5228709571500474, -24.66019654487200441, 8.947790411086119278 ) ) ;
#81334=DIRECTION ( 'NONE',  ( -3.773278334453079618E-23, 0.9999999999976377785, 2.173523156925979975E-06 ) ) ;
#81335=CARTESIAN_POINT ( 'NONE',  ( -84.62287095715008434, -23.47596703998600631, 11.44779298504227860 ) ) ;
#81336=CARTESIAN_POINT ( 'NONE',  ( -119.5228709571501184, -24.33832256527049154, 0.1851278514138659792 ) ) ;
#81338=CARTESIAN_POINT ( 'NONE',  ( -50.62287095715004881, -24.51163499207175178, 0.6490370598554262571 ) ) ;
#81339=CARTESIAN_POINT ( 'NONE',  ( -17.52048005523606022, -9.576713672051738513, 11.49999999999998934 ) ) ;
#81340=CARTESIAN_POINT ( 'NONE',  ( -59.62287095715005592, -24.50216790748100237, 0.6166512839513628164 ) ) ;
#81341=CARTESIAN_POINT ( 'NONE',  ( -0.004567304949753520950, -22.99087264824203913, 3.851531674744869349 ) ) ;
#81342=CARTESIAN_POINT ( 'NONE',  ( 19.23997954701083657, -5.074110557352235595, -1.500000000000002220 ) ) ;
#81344=CARTESIAN_POINT ( 'NONE',  ( -74.55620429048342146, -24.64898659630528854, 1.056161002820828143 ) ) ;
#81345=B_SPLINE_CURVE_WITH_KNOTS ( 'NONE', 3,
 ( #43380, #74318, #28641, #14897, #92523, #37746, #62592, #91529, #85412, #54979, #31125, #77785 ),
 .UNSPECIFIED., .F., .F.,
 ( 4, 2, 2, 2, 2, 4 ),
 ( 0.000000000000000000, 0.0004005021043489182409, 0.0008010042086978364818, 0.001201506313046754723, 0.001401757365221215036, 0.001602008417395675349 ),
 .UNSPECIFIED. ) ;
#81350=CARTESIAN_POINT ( 'NONE',  ( -16.26442346200556344, 12.93145763113255775, 11.49999999999999645 ) ) ;
#81352=CARTESIAN_POINT ( 'NONE',  ( -36.52287095715006870, -23.47593901973090169, -1.443836447538997314 ) ) ;
#81353=CARTESIAN_POINT ( 'NONE',  ( -62.62287095715004881, -23.47596703998600276, 11.44779298504227505 ) ) ;
#81354=VERTEX_POINT ( 'NONE', #94408 ) ;
#81355=DIRECTION ( 'NONE',  ( -3.773278334453079618E-23, 0.9999999999976377785, 2.173523156925979975E-06 ) ) ;
#81356=CARTESIAN_POINT ( 'NONE',  ( -127.6238341232833164, -24.34968618360935011, 0.1864209137778924386 ) ) ;
#81357=ORIENTED_EDGE ( 'NONE', *, *, #52793, .F. ) ;
#81358=CARTESIAN_POINT ( 'NONE',  ( -11.13811422090317294, 16.88724661786912762, 11.49999999999998934 ) ) ;
#81360=DIRECTION ( 'NONE',  ( -3.773278334453079030E-23, 0.9999999999976377785, 2.173523156925979128E-06 ) ) ;
#81361=CARTESIAN_POINT ( 'NONE',  ( -129.6228709571500417, -24.64898659630367916, 1.056161002820834804 ) ) ;
#81362=CARTESIAN_POINT ( 'NONE',  ( -109.6228709571500559, -23.47593901973091235, -1.443836447538999312 ) ) ;
#81363=VERTEX_POINT ( 'NONE', #24891 ) ;
#81364=CARTESIAN_POINT ( 'NONE',  ( -46.62287095715004881, -23.47596703998600276, 11.44779298504227505 ) ) ;
#81365=CARTESIAN_POINT ( 'NONE',  ( -121.6228709571500417, -29.50250786944525672, 11.44777988621622811 ) ) ;
#81366=CARTESIAN_POINT ( 'NONE',  ( -4.446071851354966853, 19.53225066162704948, -1.500000000000002220 ) ) ;
#81367=CARTESIAN_POINT ( 'NONE',  ( -14.15979099334852798, -15.53166555317341135, 11.49999999999999645 ) ) ;
#81368=LINE ( 'NONE', #58052, #76119 ) ;
#81369=CARTESIAN_POINT ( 'NONE',  ( -70.61333134823995294, -23.48786465467241058, 11.44779295918254824 ) ) ;
#81370=CARTESIAN_POINT ( 'NONE',  ( -17.20036718215007099, 13.84871166177648583, 11.49999999999998934 ) ) ;
#81371=CARTESIAN_POINT ( 'NONE',  ( -47.52287095715007581, -23.47593901973090169, -1.443836447538997092 ) ) ;
#81373=EDGE_CURVE ( 'NONE', #22334, #13993, #12425, .T. ) ;
#81375=CARTESIAN_POINT ( 'NONE',  ( -118.5895376238167245, -24.64898659630368627, 1.056161002820390937 ) ) ;
#81376=CARTESIAN_POINT ( 'NONE',  ( -70.34543693012690824, -25.04307398257883577, 7.563174194274490780 ) ) ;
#81377=CARTESIAN_POINT ( 'NONE',  ( -114.5228709571500616, -24.64965694238408034, 8.947790433994192938 ) ) ;
#81378=ADVANCED_FACE ( 'NONE', ( #87806 ), #32514, .F. ) ;
#81379=VERTEX_POINT ( 'NONE', #48250 ) ;
#81380=ADVANCED_FACE ( 'NONE', ( #95414 ), #16783, .F. ) ;
#81383=CARTESIAN_POINT ( 'NONE',  ( -80.92287095715006728, -23.47596703998600631, 11.44779298504227860 ) ) ;
#81384=CARTESIAN_POINT ( 'NONE',  ( -58.62287095715006302, -24.65952944569304250, 1.056160979905695463 ) ) ;
#81385=CARTESIAN_POINT ( 'NONE',  ( -3.210669876418242197, 20.33209092710186638, -1.500000000000002220 ) ) ;
#81387=CARTESIAN_POINT ( 'NONE',  ( -7.320277434469578459, 20.25297033093062282, 11.49999999999999645 ) ) ;
#81388=ORIENTED_EDGE ( 'NONE', *, *, #22285, .F. ) ;
#81389=DIRECTION ( 'NONE',  ( -3.773278334453080206E-23, 0.9999999999976377785, 2.173523156925979975E-06 ) ) ;
#81391=DIRECTION ( 'NONE',  ( 0.000000000000000000, 0.9999999999976377785, 2.173523156925979975E-06 ) ) ;
#81392=CARTESIAN_POINT ( 'NONE',  ( 8.793911523065595759, -20.50603677605392150, -1.500000000000002220 ) ) ;
#81393=EDGE_CURVE ( 'NONE', #72031, #15988, #82510, .T. ) ;
#81396=CARTESIAN_POINT ( 'NONE',  ( -58.62287095715007013, -23.47596703998600276, 11.44779298504227683 ) ) ;
#81398=CARTESIAN_POINT ( 'NONE',  ( -101.6228709571501128, -24.34917612406837861, 0.1852690917426677852 ) ) ;
#81400=VECTOR ( 'NONE', #95799, 1000.000000000000114 ) ;
#81401=CARTESIAN_POINT ( 'NONE',  ( 8.688630223215852766, -18.96179456382524364, 11.49999999999998934 ) ) ;
#81403=VERTEX_POINT ( 'NONE', #55871 ) ;
#81404=CARTESIAN_POINT ( 'NONE',  ( -39.73230706801754764, -25.13992894415259016, 3.001193081787598693 ) ) ;
#81406=B_SPLINE_CURVE_WITH_KNOTS ( 'NONE', 3,
 ( #79899, #782, #278, #31734, #93120, #71807 ),
 .UNSPECIFIED., .F., .F.,
 ( 4, 2, 4 ),
 ( 6.391158118963033063E-06, 0.001387004593080784194, 0.002767618028042605031 ),
 .UNSPECIFIED. ) ;
#81407=EDGE_LOOP ( 'NONE', ( #44492, #32249, #97951, #33082 ) ) ;
#81408=FACE_OUTER_BOUND ( 'NONE', #491, .T. ) ;
#81409=CARTESIAN_POINT ( 'NONE',  ( -19.68365937621761219, -7.520201837432793468, -1.500000000000002220 ) ) ;
#81412=CARTESIAN_POINT ( 'NONE',  ( -98.52287095715006160, -23.48783264082477018, -1.443836473390087916 ) ) ;
#81413=CARTESIAN_POINT ( 'NONE',  ( -105.5562042904833788, -25.00182538069145721, 7.747789668545099317 ) ) ;
#81415=CARTESIAN_POINT ( 'NONE',  ( -49.15081903914613548, -25.23404858129530126, 3.683285954327154332 ) ) ;
#81416=CARTESIAN_POINT ( 'NONE',  ( -17.03913561245058261, -13.47071831616118942, -1.500000000000002220 ) ) ;
#81417=CARTESIAN_POINT ( 'NONE',  ( -81.35928118207723969, -25.12224291375864027, 6.638486925961360363 ) ) ;
#81418=CARTESIAN_POINT ( 'NONE',  ( -7.755428854246955161, -20.87388092083558888, 11.49999999999999645 ) ) ;
#81420=CARTESIAN_POINT ( 'NONE',  ( -50.41832839342763606, -25.24728723697485577, 5.198500959637132546 ) ) ;
#81422=EDGE_CURVE ( 'NONE', #68434, #93569, #41369, .T. ) ;
#81423=DIRECTION ( 'NONE',  ( -3.773278334453079030E-23, 0.9999999999976377785, 2.173523156925979128E-06 ) ) ;
#81424=ORIENTED_EDGE ( 'NONE', *, *, #11460, .F. ) ;
#81425=CARTESIAN_POINT ( 'NONE',  ( -53.62287095715005592, -23.47593901973091235, -1.443836447539009749 ) ) ;
#81426=ORIENTED_EDGE ( 'NONE', *, *, #348, .T. ) ;
#81431=CARTESIAN_POINT ( 'NONE',  ( -117.5228709571500758, -23.48786465467241769, 11.44779295918253759 ) ) ;
#81438=CARTESIAN_POINT ( 'NONE',  ( -21.16806448877717628, 7.570426553894726851, -1.500000000000002220 ) ) ;
#81440=B_SPLINE_CURVE_WITH_KNOTS ( 'NONE', 3,
 ( #42567, #51162, #97824, #58775 ),
 .UNSPECIFIED., .F., .F.,
 ( 4, 4 ),
 ( 0.000000000000000000, 9.999999999998897304E-05 ),
 .UNSPECIFIED. ) ;
#81443=FACE_OUTER_BOUND ( 'NONE', #29105, .T. ) ;
#81445=CARTESIAN_POINT ( 'NONE',  ( -116.5228709571500900, -23.72747288104470442, -1.053458166803225460 ) ) ;
#81446=B_SPLINE_CURVE_WITH_KNOTS ( 'NONE', 3,
 ( #8892, #61203, #37845, #69796 ),
 .UNSPECIFIED., .F., .F.,
 ( 4, 4 ),
 ( 6.938893903907228378E-18, 0.0001000000000000028644 ),
 .UNSPECIFIED. ) ;
#81447=CARTESIAN_POINT ( 'NONE',  ( -63.92072118931277203, -24.75152770810919733, 1.363349870542269082 ) ) ;
#81448=EDGE_CURVE ( 'NONE', #42451, #48335, #37762, .T. ) ;
#81449=CARTESIAN_POINT ( 'NONE',  ( -0.6043519431218743465, -19.59835197619436187, -1.500000000000002220 ) ) ;
#81450=B_SPLINE_SURFACE_WITH_KNOTS ( 'NONE', 3, 3, ( 
 ( #70010, #87622, #72904, #46178 ),
 ( #3400, #18594, #18105, #31448 ),
 ( #57192, #93336, #79999, #78105 ),
 ( #65314, #33828, #1007, #495 ),
 ( #23320, #25711, #54303, #10486 ),
 ( #64815, #95730, #85231, #84730 ),
 ( #80501, #15718, #62411, #77107 ) ),
 .UNSPECIFIED., .F., .F., .F.,
 ( 4, 3, 4 ),
 ( 4, 4 ),
 ( 0.7945040050992244751, 0.8970133687736506767, 0.9995227324480768782 ),
 ( 0.7596870442490788466, 0.7610504907558764964 ),
 .UNSPECIFIED. ) ;
#81451=CARTESIAN_POINT ( 'NONE',  ( -46.66195802986739949, -23.48783264082476663, -1.443836473390096575 ) ) ;
#81452=VERTEX_POINT ( 'NONE', #9678 ) ;
#81453=B_SPLINE_CURVE_WITH_KNOTS ( 'NONE', 3,
 ( #76660, #92898, #93397, #99994, #76169, #61474, #31005, #30001 ),
 .UNSPECIFIED., .F., .F.,
 ( 4, 2, 2, 4 ),
 ( 0.000000000000000000, 0.002001098010032688855, 0.003001647015049033283, 0.004002196020065377710 ),
 .UNSPECIFIED. ) ;
#81454=CARTESIAN_POINT ( 'NONE',  ( 11.68953838083566588, 18.09531432177502808, -1.500000000000002220 ) ) ;
#81456=CARTESIAN_POINT ( 'NONE',  ( -80.88693734264360558, -25.31572658427561962, 5.024145845486627238 ) ) ;
#81457=CARTESIAN_POINT ( 'NONE',  ( -100.5895376238167245, -23.48783264082478794, -1.443836473390061936 ) ) ;
#81460=CARTESIAN_POINT ( 'NONE',  ( 16.94363762160741516, 15.55198921429254533, -1.500000000000002220 ) ) ;
#81463=CARTESIAN_POINT ( 'NONE',  ( -101.6430330839730374, -25.27307239909451653, 3.986250617436227550 ) ) ;
#81464=FACE_OUTER_BOUND ( 'NONE', #100326, .T. ) ;
#81465=CARTESIAN_POINT ( 'NONE',  ( 19.44710440357065551, 5.058846670610233076, 11.49999999999999645 ) ) ;
#81467=CARTESIAN_POINT ( 'NONE',  ( -81.88534077628074215, -25.23679622552714363, 6.293943003980942308 ) ) ;
#81469=DIRECTION ( 'NONE',  ( -3.773278334444166432E-23, 1.000000000000000000, 0.000000000000000000 ) ) ;
#81470=CARTESIAN_POINT ( 'NONE',  ( -65.62287095715002749, -24.91544648472619983, 1.928969306349235691 ) ) ;
#81471=CARTESIAN_POINT ( 'NONE',  ( -125.6228709571500559, -29.50248528299804818, 1.056150453629047137 ) ) ;
#81472=CARTESIAN_POINT ( 'NONE',  ( -18.24115112668064853, 7.888873183027880209, 11.49999999999998934 ) ) ;
#81473=CARTESIAN_POINT ( 'NONE',  ( -113.6244797112919400, -24.51314013834316086, 0.6176544820404182845 ) ) ;
#81474=CARTESIAN_POINT ( 'NONE',  ( 15.21843288076463629, 12.49332292251147614, -1.500000000000002220 ) ) ;
#81478=CARTESIAN_POINT ( 'NONE',  ( -57.52287095715005449, -24.64965694238407323, 8.947790433994201820 ) ) ;
#81480=CARTESIAN_POINT ( 'NONE',  ( 1.582324178664715975, -20.54890914157308401, 11.49999999999999645 ) ) ;
#81481=CARTESIAN_POINT ( 'NONE',  ( -128.5228709571501042, -23.73934037231758154, 11.05740245334327732 ) ) ;
#81482=CARTESIAN_POINT ( 'NONE',  ( 21.95517018727266390, 5.574673621280945568, 11.49999999999999645 ) ) ;
#81485=CARTESIAN_POINT ( 'NONE',  ( -42.62287095715006302, -23.47596703998600276, 11.44779298504227505 ) ) ;
#81486=CARTESIAN_POINT ( 'NONE',  ( -110.5228709571500900, -23.85196035786901092, -0.8779234886475162369 ) ) ;
#81488=ORIENTED_EDGE ( 'NONE', *, *, #49638, .T. ) ;
#81489=ORIENTED_EDGE ( 'NONE', *, *, #93611, .F. ) ;
#81490=VECTOR ( 'NONE', #100391, 1000.000000000000114 ) ;
#81492=CARTESIAN_POINT ( 'NONE',  ( 13.72848742581335912, -18.28091200367991576, 11.49999999999998934 ) ) ;
#81494=CARTESIAN_POINT ( 'NONE',  ( 21.32721141102669193, -3.434809268862642817, -1.500000000000002220 ) ) ;
#81495=CARTESIAN_POINT ( 'NONE',  ( -113.6255546038343596, -24.35071581493543746, 9.817618358456018157 ) ) ;
#81496=DIRECTION ( 'NONE',  ( -3.773278334453080206E-23, 0.9999999999976377785, 2.173523156925979975E-06 ) ) ;
#81498=CARTESIAN_POINT ( 'NONE',  ( 8.566404662457630437, 20.85315857434707709, 11.49999999999999645 ) ) ;
#81499=VERTEX_POINT ( 'NONE', #87296 ) ;
#81501=CARTESIAN_POINT ( 'NONE',  ( 6.372119535971386917, -21.01724095701019479, -1.500000000000002220 ) ) ;
#81502=CARTESIAN_POINT ( 'NONE',  ( -111.5905792267520127, -24.15543982623907482, -0.2315651400026575712 ) ) ;
#81503=LINE ( 'NONE', #41953, #36293 ) ;
#81504=AXIS2_PLACEMENT_3D ( 'NONE', #50268, #63119, #41664 ) ;
#81510=CARTESIAN_POINT ( 'NONE',  ( -121.6228709571500417, -29.50250243563736774, 8.947779886222134493 ) ) ;
#81511=EDGE_CURVE ( 'NONE', #7991, #89948, #24396, .T. ) ;
#81515=ORIENTED_EDGE ( 'NONE', *, *, #27057, .F. ) ;
#81519=CARTESIAN_POINT ( 'NONE',  ( 14.56535739210195857, -14.21638276092092745, -1.500000000000002220 ) ) ;
#81520=ADVANCED_FACE ( 'NONE', ( #55364 ), #78307, .T. ) ;
#81521=ORIENTED_EDGE ( 'NONE', *, *, #90780, .T. ) ;
#81522=LINE ( 'NONE', #96246, #68782 ) ;
#81523=CARTESIAN_POINT ( 'NONE',  ( -88.62287095715004170, -24.51283580621365132, 0.6167428607019744824 ) ) ;
#81525=CARTESIAN_POINT ( 'NONE',  ( -105.5100292654264393, -24.73486907724918993, 1.287355809206962576 ) ) ;
#81526=CARTESIAN_POINT ( 'NONE',  ( -71.66734858977571321, -25.03149629803908738, 6.551008863527044035 ) ) ;
#81527=EDGE_LOOP ( 'NONE', ( #81606, #97732 ) ) ;
#81528=DIRECTION ( 'NONE',  ( -3.773278334453080206E-23, 0.9999999999976377785, 2.173523156925979975E-06 ) ) ;
#81529=CARTESIAN_POINT ( 'NONE',  ( -104.5228709571500758, -24.64965694238407323, 8.947790433994194714 ) ) ;
#81532=EDGE_CURVE ( 'NONE', #22199, #13524, #60783, .T. ) ;
#81533=CARTESIAN_POINT ( 'NONE',  ( -20.46667790307254009, -3.548193229090686796, -1.500000000000002220 ) ) ;
#81537=B_SPLINE_SURFACE_WITH_KNOTS ( 'NONE', 3, 1, ( 
 ( #84816, #54888 ),
 ( #70603, #91932 ),
 ( #15805, #83821 ),
 ( #62496, #46770 ),
 ( #77690, #14300 ),
 ( #30533, #6695 ),
 ( #585, #31031 ),
 ( #37649, #99528 ),
 ( #84316, #30026 ),
 ( #31532, #77192 ),
 ( #93425, #23918 ),
 ( #53387, #14798 ),
 ( #45764, #2111 ),
 ( #41165, #64026 ),
 ( #71615, #94941 ) ),
 .UNSPECIFIED., .F., .F., .F.,
 ( 4, 1, 1, 1, 1, 1, 1, 1, 1, 1, 1, 1, 4 ),
 ( 2, 2 ),
 ( 0.000000000000000000, 0.07964825118022765549, 0.1589216764181120567, 0.2396194947370321737, 0.3226094298185629428, 0.4060346366179267696, 0.4876020954923867556, 0.5696846265959313316, 0.6530361450088354447, 0.7374357177222916615, 0.8224778158555117180, 0.9097476551184092708, 1.000000000000000000 ),
 ( 0.000000000000000000, 1.000000000000000000 ),
 .UNSPECIFIED. ) ;
#81538=CARTESIAN_POINT ( 'NONE',  ( -86.62287095715008434, -23.96127896941632685, -0.6493128931037817075 ) ) ;
#81539=CARTESIAN_POINT ( 'NONE',  ( -97.52287095715009002, -24.51387760970724372, 9.387446482453396968 ) ) ;
#81540=ORIENTED_EDGE ( 'NONE', *, *, #40806, .F. ) ;
#81545=CARTESIAN_POINT ( 'NONE',  ( -71.24017339641436308, -25.31201710090048707, 5.863458149974889011 ) ) ;
#81546=CARTESIAN_POINT ( 'NONE',  ( 14.53198226072946220, 16.64418356588832992, 11.49999999999999645 ) ) ;
#81547=ORIENTED_EDGE ( 'NONE', *, *, #13559, .T. ) ;
#81548=CARTESIAN_POINT ( 'NONE',  ( -113.5228709571500616, -24.64898659630368627, 1.056161002820831474 ) ) ;
#81549=AXIS2_PLACEMENT_3D ( 'NONE', #77877, #29227, #60195 ) ;
#81550=CARTESIAN_POINT ( 'NONE',  ( -22.51868310087907687, -2.221351303042197411, -1.500000000000002220 ) ) ;
#81551=CARTESIAN_POINT ( 'NONE',  ( -115.6256581184850774, -24.63419186844613051, 9.035850630976923981 ) ) ;
#81554=ORIENTED_EDGE ( 'NONE', *, *, #728, .F. ) ;
#81556=CARTESIAN_POINT ( 'NONE',  ( -57.63243796231297722, -24.35071581493543036, 9.817618358456028815 ) ) ;
#81558=CARTESIAN_POINT ( 'NONE',  ( -6.202713861520617655, -20.23501359363181962, -1.500000000000002220 ) ) ;
#81561=CARTESIAN_POINT ( 'NONE',  ( 13.23790625878087468, -17.95846084735695314, -1.500000000000002220 ) ) ;
#81562=CARTESIAN_POINT ( 'NONE',  ( -46.62287095715004881, -23.47593901973091235, -1.443836447539009749 ) ) ;
#81566=CARTESIAN_POINT ( 'NONE',  ( -111.5562042904833788, -24.65952944569305316, 1.056160979905704567 ) ) ;
#81569=CARTESIAN_POINT ( 'NONE',  ( -16.16875682573952133, 10.94412424577950915, 11.49999999999998934 ) ) ;
#81570=CARTESIAN_POINT ( 'NONE',  ( 2.169945595249806125, 21.32849103866527329, -1.500000000000002220 ) ) ;
#81571=CARTESIAN_POINT ( 'NONE',  ( -26.36451126669314604, -24.92774786267114351, 2.180457190752079999 ) ) ;
#81572=CARTESIAN_POINT ( 'NONE',  ( -60.62287095715004881, -29.50250786944525672, 11.44777988621623876 ) ) ;
#81573=CARTESIAN_POINT ( 'NONE',  ( -77.64774600778000035, -23.48783264082476663, -1.443836473390097241 ) ) ;
#81575=CARTESIAN_POINT ( 'NONE',  ( -18.62658236799572720, 13.20813282334384553, -1.500000000000002220 ) ) ;
#81576=VECTOR ( 'NONE', #81967, 1000.000000000000114 ) ;
#81577=EDGE_CURVE ( 'NONE', #1598, #77838, #8652, .T. ) ;
#81579=CARTESIAN_POINT ( 'NONE',  ( -106.6282279683493357, -24.15620529776629510, 10.23563542870659582 ) ) ;
#81581=CARTESIAN_POINT ( 'NONE',  ( 1.402406813841059030, 19.88454085074057076, 11.49999999999999645 ) ) ;
#81582=CARTESIAN_POINT ( 'NONE',  ( -104.5872775516450162, -24.51314013834316796, 0.6176544820404187286 ) ) ;
#81584=CARTESIAN_POINT ( 'NONE',  ( -88.88918693012689687, -25.27880950044345454, 5.947789066509454159 ) ) ;
#81585=CARTESIAN_POINT ( 'NONE',  ( -101.6228709571500559, -23.47593901973091235, -1.443836447539001089 ) ) ;
#81588=CARTESIAN_POINT ( 'NONE',  ( -62.62287095715004881, -23.72773821059535848, 11.05748984161097503 ) ) ;
#81589=CARTESIAN_POINT ( 'NONE',  ( -1.268225406894735396, -21.67698866206750097, -1.500000000000002220 ) ) ;
#81591=CARTESIAN_POINT ( 'NONE',  ( -19.30006219055749739, -3.230038287793697283, -1.500000000000002220 ) ) ;
#81594=CARTESIAN_POINT ( 'NONE',  ( 20.25987197511681259, 2.754759976156288204, 11.49999999999999645 ) ) ;
#81595=CARTESIAN_POINT ( 'NONE',  ( -50.37830952628070946, -25.30401792888237367, 5.197789011716579033 ) ) ;
#81596=ADVANCED_FACE ( 'NONE', ( #51745 ), #51237, .F. ) ;
#81597=CARTESIAN_POINT ( 'NONE',  ( -108.8968792378191921, -29.50249817218807635, 6.986241424688308221 ) ) ;
#81598=B_SPLINE_CURVE_WITH_KNOTS ( 'NONE', 3,
 ( #71041, #41094, #32978, #9128 ),
 .UNSPECIFIED., .F., .F.,
 ( 4, 4 ),
 ( 0.000000000000000000, 0.0001000000000000028644 ),
 .UNSPECIFIED. ) ;
#81599=ORIENTED_EDGE ( 'NONE', *, *, #93430, .F. ) ;
#81601=DIRECTION ( 'NONE',  ( 1.000000000000000000, 3.773278334444167608E-23, 8.201307833595939069E-29 ) ) ;
#81604=PLANE ( 'NONE',  #87305 ) ;
#81606=ORIENTED_EDGE ( 'NONE', *, *, #93858, .T. ) ;
#81607=CARTESIAN_POINT ( 'NONE',  ( -79.11611000704996854, -25.14083923594767001, 2.947789366383933185 ) ) ;
#81608=CARTESIAN_POINT ( 'NONE',  ( -5.582908757718670678, 22.30220962497079285, 11.49999999999999645 ) ) ;
#81609=CARTESIAN_POINT ( 'NONE',  ( -0.9122204482399535186, 22.77315974801211240, -1.500000000000002220 ) ) ;
#81610=CARTESIAN_POINT ( 'NONE',  ( -70.70614159023084255, -25.05208580739551039, 7.521011471076567645 ) ) ;
#81611=AXIS2_PLACEMENT_3D ( 'NONE', #3397, #50062, #12973 ) ;
#81612=CARTESIAN_POINT ( 'NONE',  ( -40.52287095715004028, -24.82558206586148941, 1.605769216559624457 ) ) ;
#81613=FACE_OUTER_BOUND ( 'NONE', #42833, .T. ) ;
#81614=CARTESIAN_POINT ( 'NONE',  ( -78.62287095715004170, -23.48786465467241413, 11.44779295918254469 ) ) ;
#81616=CARTESIAN_POINT ( 'NONE',  ( -21.85961425739535358, 0.8689724601130633941, -1.500000000000002220 ) ) ;
#81617=PLANE ( 'NONE',  #68911 ) ;
#81618=CARTESIAN_POINT ( 'NONE',  ( -67.62287095715005592, -29.50250786944525672, 11.44777988621623699 ) ) ;
#81619=CARTESIAN_POINT ( 'NONE',  ( -71.50915260164352105, -25.29966242988960090, 5.397575489595221931 ) ) ;
#81621=ORIENTED_EDGE ( 'NONE', *, *, #53351, .F. ) ;
#81622=CARTESIAN_POINT ( 'NONE',  ( 12.15263457413992576, -16.39098610538439615, -1.500000000000002220 ) ) ;
#81623=ORIENTED_EDGE ( 'NONE', *, *, #89891, .F. ) ;
#81626=EDGE_LOOP ( 'NONE', ( #247, #81839, #67710, #12014 ) ) ;
#81627=B_SPLINE_CURVE_WITH_KNOTS ( 'NONE', 3,
 ( #77729, #86367, #16851, #8244 ),
 .UNSPECIFIED., .F., .F.,
 ( 4, 4 ),
 ( 0.000000000000000000, 0.0001000000000000167422 ),
 .UNSPECIFIED. ) ;
#81628=CARTESIAN_POINT ( 'NONE',  ( -11.96207688724106610, 19.68918167733909641, -1.500000000000002220 ) ) ;
#81629=DIRECTION ( 'NONE',  ( -3.773278334453080206E-23, 0.9999999999976377785, 2.173523156925979975E-06 ) ) ;
#81630=CARTESIAN_POINT ( 'NONE',  ( 20.19498477198788322, 0.2509159868347127231, -1.500000000000002220 ) ) ;
#81631=EDGE_CURVE ( 'NONE', #47607, #16500, #26805, .T. ) ;
#81633=CARTESIAN_POINT ( 'NONE',  ( -69.55620429048340725, -23.47596703998600276, 11.44779298504227505 ) ) ;
#81634=CARTESIAN_POINT ( 'NONE',  ( -34.55620429048339304, -24.64965694238574656, 8.947790433994203596 ) ) ;
#81635=DIRECTION ( 'NONE',  ( 0.000000000000000000, -2.173523156925979552E-06, 0.9999999999976378895 ) ) ;
#81637=CARTESIAN_POINT ( 'NONE',  ( 20.27498964588844643, 6.839650151297337999, 11.49999999999999645 ) ) ;
#81640=ADVANCED_FACE ( 'NONE', ( #5059 ), #44129, .F. ) ;
#81642=CARTESIAN_POINT ( 'NONE',  ( 10.43072250204971851, -19.66636941823637841, -1.500000000000002220 ) ) ;
#81643=EDGE_CURVE ( 'NONE', #84023, #34094, #92207, .T. ) ;
#81644=CARTESIAN_POINT ( 'NONE',  ( -17.26476610439243231, 11.37957233835482818, -1.500000000000002220 ) ) ;
#81646=ORIENTED_EDGE ( 'NONE', *, *, #3748, .T. ) ;
#81653=CARTESIAN_POINT ( 'NONE',  ( -12.66259425867894350, -16.64798919286708667, -1.500000000000002220 ) ) ;
#81655=CARTESIAN_POINT ( 'NONE',  ( -12.72821696145241255, -17.84489267850806726, 11.49999999999999645 ) ) ;
#81656=CARTESIAN_POINT ( 'NONE',  ( -107.6228709571500701, -24.66019654487199730, 8.947790411086124607 ) ) ;
#81657=CARTESIAN_POINT ( 'NONE',  ( 3.368619518803146029, -22.26131067175759881, -1.500000000000002220 ) ) ;
#81658=CARTESIAN_POINT ( 'NONE',  ( 19.95448254803897115, -6.385634049875297258, -1.500000000000002220 ) ) ;
#81659=CARTESIAN_POINT ( 'NONE',  ( -38.53901505288835239, -24.34968618360933590, 0.1864209137778850278 ) ) ;
#81661=CARTESIAN_POINT ( 'NONE',  ( -119.6256459593364383, -24.15620529776629510, 10.23563542870659582 ) ) ;
#81662=CARTESIAN_POINT ( 'NONE',  ( -32.50560602629348494, -24.87219037988797865, 1.747789950295646877 ) ) ;
#81664=VERTEX_POINT ( 'NONE', #83676 ) ;
#81666=CARTESIAN_POINT ( 'NONE',  ( -44.52287095715008292, -23.96177878511308990, 10.65340807706330395 ) ) ;
#81667=ORIENTED_EDGE ( 'NONE', *, *, #64019, .T. ) ;
#81668=CARTESIAN_POINT ( 'NONE',  ( 18.29419249859179786, 11.19154738541161365, -1.500000000000002220 ) ) ;
#81669=CARTESIAN_POINT ( 'NONE',  ( -95.58953762381672448, -23.47593901973091235, -1.443836447539001089 ) ) ;
#81670=VERTEX_POINT ( 'NONE', #61861 ) ;
#81671=CARTESIAN_POINT ( 'NONE',  ( 20.99878002148846790, -2.064974809011826729, -1.500000000000002220 ) ) ;
#81672=CARTESIAN_POINT ( 'NONE',  ( -92.55620429048339304, -24.64965694238574656, 8.947790433994201820 ) ) ;
#81674=CARTESIAN_POINT ( 'NONE',  ( -50.60991402953558804, -23.85049219812685095, 10.88485053497527133 ) ) ;
#81675=LINE ( 'NONE', #96898, #58843 ) ;
#81676=CARTESIAN_POINT ( 'NONE',  ( -109.4926097204045163, -25.31342473612490096, 4.739357423808571390 ) ) ;
#81677=CARTESIAN_POINT ( 'NONE',  ( -12.21066354923914865, 18.40238043084326591, -1.500000000000002220 ) ) ;
#81680=B_SPLINE_CURVE_WITH_KNOTS ( 'NONE', 3,
 ( #38364, #30752, #8915, #92643 ),
 .UNSPECIFIED., .F., .F.,
 ( 4, 4 ),
 ( 0.000000000000000000, 9.999999999997510880E-05 ),
 .UNSPECIFIED. ) ;
#81681=VECTOR ( 'NONE', #49936, 1000.000000000000114 ) ;
#81682=CARTESIAN_POINT ( 'NONE',  ( -51.90278039571972357, -25.31633292683138237, 5.898133778068365807 ) ) ;
#81683=CARTESIAN_POINT ( 'NONE',  ( -40.53889064818358889, -25.31624741514509935, 5.542732875838958684 ) ) ;
#81685=CARTESIAN_POINT ( 'NONE',  ( -25.51311700692786388, -24.74886220813050031, 2.662461283694073089 ) ) ;
#81687=CARTESIAN_POINT ( 'NONE',  ( -63.52287095715010423, -23.96127896941632329, -0.6493128931038021356 ) ) ;
#81688=CARTESIAN_POINT ( 'NONE',  ( 13.79380260783658407, 16.28676726024703214, -1.500000000000002220 ) ) ;
#81689=CARTESIAN_POINT ( 'NONE',  ( -26.25113031250881690, -24.91578880384921391, 6.269870734223003339 ) ) ;
#81690=CARTESIAN_POINT ( 'NONE',  ( -50.91630580738321754, -25.32724633150699489, 4.398074151685129607 ) ) ;
#81691=EDGE_CURVE ( 'NONE', #93833, #70270, #54664, .T. ) ;
#81692=CARTESIAN_POINT ( 'NONE',  ( -86.62287095715004170, -24.64898659630528854, 1.056161002820827921 ) ) ;
#81693=DIRECTION ( 'NONE',  ( -1.000000000000000000, -3.773278334444167608E-23, -8.201307833595939069E-29 ) ) ;
#81694=CARTESIAN_POINT ( 'NONE',  ( 17.19246737676917292, 14.74310579602587090, -1.500000000000002220 ) ) ;
#81695=CARTESIAN_POINT ( 'NONE',  ( -32.92287095715006018, -23.47596703998600276, 11.44779298504227683 ) ) ;
#81696=VERTEX_POINT ( 'NONE', #52737 ) ;
#81699=CARTESIAN_POINT ( 'NONE',  ( -18.42202159362721048, -7.168033771007030097, 11.49999999999999645 ) ) ;
#81700=CARTESIAN_POINT ( 'NONE',  ( -122.5228709571500616, -24.66019654487200441, 8.947790411086112172 ) ) ;
#81701=CARTESIAN_POINT ( 'NONE',  ( -32.07722060962682775, -25.11010177581465186, 2.831122766525584478 ) ) ;
#81703=FACE_OUTER_BOUND ( 'NONE', #73067, .T. ) ;
#81704=CARTESIAN_POINT ( 'NONE',  ( -28.91304442625643034, -24.60093986950708356, 2.072904486375534816 ) ) ;
#81705=CARTESIAN_POINT ( 'NONE',  ( -113.5895376238167245, -24.64898659630368627, 1.056161002820388717 ) ) ;
#81706=CARTESIAN_POINT ( 'NONE',  ( -20.67203406374276398, -6.343553224398504220, 11.49999999999998934 ) ) ;
#81707=CARTESIAN_POINT ( 'NONE',  ( -106.5228709571500758, -24.65952944569305316, 1.056160979905704123 ) ) ;
#81708=CARTESIAN_POINT ( 'NONE',  ( -19.35591191756920892, -0.7100623379298715010, -1.500000000000002220 ) ) ;
#81711=CARTESIAN_POINT ( 'NONE',  ( -14.06767371131996214, 13.90018863433869889, -1.500000000000002220 ) ) ;
#81713=CARTESIAN_POINT ( 'NONE',  ( 20.02926185082240451, -2.967945350358753398, 11.49999999999999645 ) ) ;
#81714=CARTESIAN_POINT ( 'NONE',  ( -119.5228709571500900, -24.51387760970726148, 9.387446482453405849 ) ) ;
#81716=LINE ( 'NONE', #58394, #42521 ) ;
#81718=B_SPLINE_SURFACE_WITH_KNOTS ( 'NONE', 3, 3, ( 
 ( #7660, #8165, #71074, #10168 ),
 ( #55857, #32504, #42139, #72083 ),
 ( #87283, #49750, #48747, #33501 ),
 ( #18279, #24880, #86783, #64985 ),
 ( #73079, #3069, #33009, #71577 ),
 ( #56863, #63476, #96401, #9669 ),
 ( #11164, #57365, #88297, #63984 ),
 ( #50238, #95899, #26395, #2565 ),
 ( #1564, #18768, #49251, #26891 ),
 ( #40623, #95402, #57863, #81177 ) ),
 .UNSPECIFIED., .F., .F., .F.,
 ( 4, 3, 3, 4 ),
 ( 4, 4 ),
 ( 0.7022005934544806038, 0.7765311282028795059, 0.8508616629512784080, 0.9995227324480763231 ),
 ( 0.6495723911733531919, 0.6509722519778085026 ),
 .UNSPECIFIED. ) ;
#81719=CARTESIAN_POINT ( 'NONE',  ( -100.1844657475011218, -25.30123273641313375, 4.676267690568757907 ) ) ;
#81722=CARTESIAN_POINT ( 'NONE',  ( -92.62287095715005592, -24.66019654487199730, 8.947790411086124607 ) ) ;
#81724=CARTESIAN_POINT ( 'NONE',  ( 12.62869658624171976, -15.57725692549414376, 11.49999999999998934 ) ) ;
#81727=EDGE_CURVE ( 'NONE', #84492, #65087, #31640, .T. ) ;
#81728=CARTESIAN_POINT ( 'NONE',  ( -103.5228709571500758, -24.51387760970725083, 9.387446482453407626 ) ) ;
#81729=CARTESIAN_POINT ( 'NONE',  ( -82.52287095715006160, -24.65952944569304606, 1.056160979905698794 ) ) ;
#81730=PLANE ( 'NONE',  #59773 ) ;
#81734=CARTESIAN_POINT ( 'NONE',  ( -49.26280096340228454, -25.29440776045719730, 5.833784451200525467 ) ) ;
#81735=ORIENTED_EDGE ( 'NONE', *, *, #98908, .F. ) ;
#81736=CARTESIAN_POINT ( 'NONE',  ( 5.487062353440709472, 19.58251264919930534, -1.500000000000002220 ) ) ;
#81739=CARTESIAN_POINT ( 'NONE',  ( -20.69623851537618364, -9.862649113751288610, -1.500000000000002220 ) ) ;
#81743=CARTESIAN_POINT ( 'NONE',  ( -108.5228709571500758, -24.35013146730204170, 9.818937971375099494 ) ) ;
#81745=B_SPLINE_CURVE_WITH_KNOTS ( 'NONE', 3,
 ( #7511, #88152, #2417, #26745, #41989, #18621 ),
 .UNSPECIFIED., .F., .F.,
 ( 4, 2, 4 ),
 ( 0.000000000000000000, 0.001380764517853252720, 0.002761529035706505441 ),
 .UNSPECIFIED. ) ;
#81747=CARTESIAN_POINT ( 'NONE',  ( 16.91677535067316995, -12.78530099663392505, 11.49999999999999645 ) ) ;
#81749=CARTESIAN_POINT ( 'NONE',  ( -5.843409716339609261, -21.38298466452703650, -1.500000000000002220 ) ) ;
#81750=EDGE_CURVE ( 'NONE', #97480, #7329, #1480, .T. ) ;
#81751=CARTESIAN_POINT ( 'NONE',  ( -7.762539992054180438, 19.06225842855939234, 11.49999999999998934 ) ) ;
#81752=B_SPLINE_CURVE_WITH_KNOTS ( 'NONE', 3,
 ( #18364, #49332, #26486, #71658, #10757, #2157 ),
 .UNSPECIFIED., .F., .F.,
 ( 4, 2, 4 ),
 ( 1.570755371633856203E-05, 0.001396183895866086235, 0.002776660238015833844 ),
 .UNSPECIFIED. ) ;
#81758=ORIENTED_EDGE ( 'NONE', *, *, #58768, .F. ) ;
#81760=CARTESIAN_POINT ( 'NONE',  ( -116.6228709571500701, -24.50321055353807864, 9.387540953477524042 ) ) ;
#81761=CARTESIAN_POINT ( 'NONE',  ( -46.52287095715008292, -23.72747288104470442, -1.053458166803227680 ) ) ;
#81762=LINE ( 'NONE', #97484, #77847 ) ;
#81763=CARTESIAN_POINT ( 'NONE',  ( 6.705275102110877405, 19.67741782454948662, -1.500000000000002220 ) ) ;
#81765=CARTESIAN_POINT ( 'NONE',  ( 0.4029737066630413311, -21.70969715354747009, 11.49999999999999645 ) ) ;
#81768=CARTESIAN_POINT ( 'NONE',  ( -115.5200949002220767, -23.85016227208580730, -0.8807180028928282001 ) ) ;
#81769=CARTESIAN_POINT ( 'NONE',  ( -10.09097066620046235, 20.03973272787133553, 11.49999999999998934 ) ) ;
#81770=CARTESIAN_POINT ( 'NONE',  ( -33.55620429048339304, -24.64965694238574656, 8.947790433994208925 ) ) ;
#81772=ORIENTED_EDGE ( 'NONE', *, *, #64232, .T. ) ;
#81774=DIRECTION ( 'NONE',  ( 0.000000000000000000, -0.9999999999976377785, -2.173523156925979128E-06 ) ) ;
#81775=AXIS2_PLACEMENT_3D ( 'NONE', #37408, #84066, #45027 ) ;
#81777=ORIENTED_EDGE ( 'NONE', *, *, #61904, .T. ) ;
#81778=FACE_OUTER_BOUND ( 'NONE', #74302, .T. ) ;
#81779=EDGE_LOOP ( 'NONE', ( #31927, #84147, #94855, #93218 ) ) ;
#81780=B_SPLINE_CURVE_WITH_KNOTS ( 'NONE', 3,
 ( #78647, #61956, #79165, #71574 ),
 .UNSPECIFIED., .F., .F.,
 ( 4, 4 ),
 ( 0.000000000000000000, 9.999999999998897304E-05 ),
 .UNSPECIFIED. ) ;
#81781=B_SPLINE_CURVE_WITH_KNOTS ( 'NONE', 3,
 ( #87747, #1010, #24339, #85740, #31955, #71026 ),
 .UNSPECIFIED., .F., .F.,
 ( 4, 2, 4 ),
 ( 6.391158118970788496E-06, 0.001387004593080793302, 0.002767618028042615873 ),
 .UNSPECIFIED. ) ;
#81782=CARTESIAN_POINT ( 'NONE',  ( -3.453506354162970915, -21.03206338698385736, -1.500000000000002220 ) ) ;
#81784=CARTESIAN_POINT ( 'NONE',  ( -88.59478540386743362, -23.96119346886881019, -0.6495511937832099125 ) ) ;
#81785=CARTESIAN_POINT ( 'NONE',  ( -5.042499505632127565, 21.24692939306837758, 11.49999999999998934 ) ) ;
#81787=CARTESIAN_POINT ( 'NONE',  ( 22.03932947713327906, 5.445304565557160359, 11.49999999999998934 ) ) ;
#81788=CARTESIAN_POINT ( 'NONE',  ( -41.44993916608342488, -25.28892577674693598, 4.009750349030761107 ) ) ;
#81789=CARTESIAN_POINT ( 'NONE',  ( -35.62287095715005592, -24.99132157543083821, 2.256160258750667502 ) ) ;
#81790=CARTESIAN_POINT ( 'NONE',  ( 18.54397492014093984, 11.73900455106235086, -1.500000000000002220 ) ) ;
#81793=CARTESIAN_POINT ( 'NONE',  ( -122.5545124863704416, -24.35071581493544102, 9.817618358456019934 ) ) ;
#81794=CARTESIAN_POINT ( 'NONE',  ( -49.00533630786537032, -25.12782636286262417, 6.749866211151510420 ) ) ;
#81796=CARTESIAN_POINT ( 'NONE',  ( -99.62287095715001328, -24.33927499327854704, 9.819080762295815390 ) ) ;
#81797=ORIENTED_EDGE ( 'NONE', *, *, #34311, .T. ) ;
#81799=CARTESIAN_POINT ( 'NONE',  ( -0.02086824871851778590, -22.77984412121519142, 2.712351064733613537 ) ) ;
#81800=CARTESIAN_POINT ( 'NONE',  ( 19.37530031839547107, -8.734557088507903799, -1.500000000000002220 ) ) ;
#81801=CARTESIAN_POINT ( 'NONE',  ( -112.5952074097005209, -23.48783264082478794, -1.443836473390061492 ) ) ;
#81802=CARTESIAN_POINT ( 'NONE',  ( -26.63407156546748311, -24.75186084215640037, 2.799621796061711798 ) ) ;
#81804=CARTESIAN_POINT ( 'NONE',  ( -85.49558519425330871, -25.00158670708911046, 2.256160236439219702 ) ) ;
#81805=B_SPLINE_CURVE_WITH_KNOTS ( 'NONE', 3,
 ( #44708, #89878, #36093, #13737 ),
 .UNSPECIFIED., .F., .F.,
 ( 4, 4 ),
 ( 0.000000000000000000, 0.0001000000000000028644 ),
 .UNSPECIFIED. ) ;
#81806=CARTESIAN_POINT ( 'NONE',  ( -84.62287095715004170, -24.51387760970723662, 9.387446482453407626 ) ) ;
#81808=CARTESIAN_POINT ( 'NONE',  ( -117.5936860851973762, -23.48786465467241769, 11.44779295918253581 ) ) ;
#81809=ORIENTED_EDGE ( 'NONE', *, *, #45791, .T. ) ;
#81810=CARTESIAN_POINT ( 'NONE',  ( -9.542874777335924819, 17.09510996321218101, 11.49999999999999645 ) ) ;
#81812=CARTESIAN_POINT ( 'NONE',  ( -79.37931354260665273, -25.24055654816928396, 6.260468804161273937 ) ) ;
#81813=B_SPLINE_CURVE_WITH_KNOTS ( 'NONE', 3,
 ( #9104, #53411, #84336, #40063, #53910, #45790 ),
 .UNSPECIFIED., .F., .F.,
 ( 4, 2, 4 ),
 ( 0.000000000000000000, 0.001380764517854761930, 0.002761529035709523860 ),
 .UNSPECIFIED. ) ;
#81814=ORIENTED_EDGE ( 'NONE', *, *, #34733, .F. ) ;
#81817=CARTESIAN_POINT ( 'NONE',  ( -44.58953762381671027, -24.65952944569304250, 1.056160979905695463 ) ) ;
#81818=CARTESIAN_POINT ( 'NONE',  ( -116.5562042904833930, -23.48783264082479150, -1.443836473390057940 ) ) ;
#81820=CARTESIAN_POINT ( 'NONE',  ( -106.6228709571500559, -23.48783264082479150, -1.443836473390060382 ) ) ;
#81821=CARTESIAN_POINT ( 'NONE',  ( 18.28535361393070957, 7.309334553982634652, -1.500000000000002220 ) ) ;
#81824=CARTESIAN_POINT ( 'NONE',  ( -56.52287095715006870, -29.50250243563736774, 8.947779886222145151 ) ) ;
#81828=CARTESIAN_POINT ( 'NONE',  ( -48.62287095715004881, -23.47593901973091235, -1.443836447539009749 ) ) ;
#81829=CARTESIAN_POINT ( 'NONE',  ( -125.6228709571500559, -23.47593901973091235, -1.443836447538995760 ) ) ;
#81830=CARTESIAN_POINT ( 'NONE',  ( -69.62287095715005592, -24.64898659630528854, 1.056161002820824368 ) ) ;
#81831=CARTESIAN_POINT ( 'NONE',  ( -118.5523306988183521, -24.65952944569305316, 1.056160979905708119 ) ) ;
#81832=CARTESIAN_POINT ( 'NONE',  ( -31.62287095715005236, -24.33927499327853639, 9.819080762295824272 ) ) ;
#81833=EDGE_CURVE ( 'NONE', #62812, #71428, #19612, .T. ) ;
#81835=CARTESIAN_POINT ( 'NONE',  ( -50.62287095715004170, -24.14321612903114556, -0.2833117244521691780 ) ) ;
#81836=CARTESIAN_POINT ( 'NONE',  ( 19.59856454566043382, -3.714209461170434157, -1.500000000000002220 ) ) ;
#81838=CARTESIAN_POINT ( 'NONE',  ( -0.06129594755597236877, -22.25647579004533583, 0.6535302041569640563 ) ) ;
#81839=ORIENTED_EDGE ( 'NONE', *, *, #56467, .T. ) ;
#81840=EDGE_CURVE ( 'NONE', #24865, #52488, #70484, .T. ) ;
#81841=CARTESIAN_POINT ( 'NONE',  ( -112.6228709571500701, -23.48783264082479150, -1.443836473390060160 ) ) ;
#81843=EDGE_CURVE ( 'NONE', #35617, #62726, #57211, .T. ) ;
#81844=EDGE_CURVE ( 'NONE', #53767, #17423, #42641, .T. ) ;
#81845=VECTOR ( 'NONE', #74224, 1000.000000000000114 ) ;
#81847=CARTESIAN_POINT ( 'NONE',  ( -49.62287095715005592, -24.51387760970723662, 9.387446482453421837 ) ) ;
#81848=CARTESIAN_POINT ( 'NONE',  ( -63.62287095715004881, -29.50248528299804818, 1.056150453629034924 ) ) ;
#81849=CARTESIAN_POINT ( 'NONE',  ( -26.19271238903531085, -24.92001040704539250, 3.794289475298080028 ) ) ;
#81850=CARTESIAN_POINT ( 'NONE',  ( -88.62287095715002749, -24.50216790748099527, 0.6166512839513722533 ) ) ;
#81852=PLANE ( 'NONE',  #47883 ) ;
#81853=CARTESIAN_POINT ( 'NONE',  ( -46.52287095715007581, -23.47593901973090524, -1.443836447538997314 ) ) ;
#81855=B_SPLINE_CURVE_WITH_KNOTS ( 'NONE', 3,
 ( #62023, #76712, #9220, #41702, #41190, #72645, #94464, #24945 ),
 .UNSPECIFIED., .F., .F.,
 ( 4, 2, 2, 4 ),
 ( -0.001224873891641419139, -0.0002244903592271050262, 0.0007758931731872090870, 0.002776660238015837313 ),
 .UNSPECIFIED. ) ;
#81856=CARTESIAN_POINT ( 'NONE',  ( 2.165584020960389822, 20.11889322763239107, -1.500000000000002220 ) ) ;
#81859=LINE ( 'NONE', #11839, #46393 ) ;
#81861=ORIENTED_EDGE ( 'NONE', *, *, #29975, .F. ) ;
#81862=CARTESIAN_POINT ( 'NONE',  ( -79.76923701135288525, -25.31526207978247811, 5.130284102396473145 ) ) ;
#81864=CARTESIAN_POINT ( 'NONE',  ( -0.1815635828756200498, -20.05798930676971636, -1.500000000000002220 ) ) ;
#81865=CARTESIAN_POINT ( 'NONE',  ( 2.184583272949580213, -20.89682302726931340, 11.49999999999999645 ) ) ;
#81868=CARTESIAN_POINT ( 'NONE',  ( -19.11006845027251799, 11.06304553819242642, 11.49999999999998934 ) ) ;
#81869=EDGE_CURVE ( 'NONE', #50913, #58306, #64378, .T. ) ;
#81870=CARTESIAN_POINT ( 'NONE',  ( -53.58953762381671737, -24.64965694238574656, 8.947790433994201820 ) ) ;
#81871=CARTESIAN_POINT ( 'NONE',  ( -107.6228709571500701, -24.64965695001469115, 8.947790433994176951 ) ) ;
#81872=CARTESIAN_POINT ( 'NONE',  ( -50.10737344585005815, -25.18440108260957899, 3.323112688921421753 ) ) ;
#81873=VERTEX_POINT ( 'NONE', #79061 ) ;
#81874=EDGE_CURVE ( 'NONE', #41093, #71061, #39025, .T. ) ;
#81875=CARTESIAN_POINT ( 'NONE',  ( -35.52287095715007581, -24.63345952396254290, 9.038047939301508293 ) ) ;
#81876=CARTESIAN_POINT ( 'NONE',  ( -38.52287095715006870, -29.50250786944525672, 11.44777988621624232 ) ) ;
#81878=ORIENTED_EDGE ( 'NONE', *, *, #32391, .T. ) ;
#81879=CARTESIAN_POINT ( 'NONE',  ( -42.62287095715006302, -23.47596703998600276, 11.44779298504227505 ) ) ;
#81881=CARTESIAN_POINT ( 'NONE',  ( -91.62287095715004170, -24.65952944569304606, 1.056160979905700792 ) ) ;
#81882=CARTESIAN_POINT ( 'NONE',  ( 6.226698476505521995, -19.64469265145860177, -1.500000000000002220 ) ) ;
#81884=CARTESIAN_POINT ( 'NONE',  ( 8.792760106793807040, 19.66521392739144858, 11.49999999999999645 ) ) ;
#81885=ORIENTED_EDGE ( 'NONE', *, *, #57736, .F. ) ;
#81889=CARTESIAN_POINT ( 'NONE',  ( 13.91197278145025074, 17.48688927191260234, 11.49999999999998934 ) ) ;
#81893=DIRECTION ( 'NONE',  ( 0.000000000000000000, -2.173523156925980399E-06, 0.9999999999976378895 ) ) ;
#81894=ORIENTED_EDGE ( 'NONE', *, *, #83832, .T. ) ;
#81895=ADVANCED_FACE ( 'NONE', ( #55252 ), #63373, .T. ) ;
#81898=CARTESIAN_POINT ( 'NONE',  ( 11.28189403632909915, 17.58240144430209995, 11.49999999999998934 ) ) ;
#81900=FACE_OUTER_BOUND ( 'NONE', #68777, .T. ) ;
#81901=VERTEX_POINT ( 'NONE', #71472 ) ;
#81902=ORIENTED_EDGE ( 'NONE', *, *, #61904, .F. ) ;
#81903=CARTESIAN_POINT ( 'NONE',  ( -100.5937251445320157, -24.15602025860896518, 10.28564288303536856 ) ) ;
#81904=CARTESIAN_POINT ( 'NONE',  ( -21.11812214938331422, 0.5215410354952813021, -1.500000000000002220 ) ) ;
#81906=CARTESIAN_POINT ( 'NONE',  ( -37.55620429048340014, -23.47596703998600276, 11.44779298504227505 ) ) ;
#81908=CARTESIAN_POINT ( 'NONE',  ( -48.62287095715006302, -23.96177878511307568, 10.65340807706330217 ) ) ;
#81909=FACE_OUTER_BOUND ( 'NONE', #1047, .T. ) ;
#81910=CARTESIAN_POINT ( 'NONE',  ( -49.28237063580810684, -25.19919229018893247, 3.391011315159921047 ) ) ;
#81911=CARTESIAN_POINT ( 'NONE',  ( -3.653784360050144286, 21.42803128968991544, -1.500000000000002220 ) ) ;
#81912=CARTESIAN_POINT ( 'NONE',  ( -81.35928118207723969, -25.24759704261755289, 6.638486653501257884 ) ) ;
#81913=CARTESIAN_POINT ( 'NONE',  ( -7.359855604737914447, 20.98419016808480109, 11.49999999999999645 ) ) ;
#81914=ORIENTED_EDGE ( 'NONE', *, *, #22920, .F. ) ;
#81915=CARTESIAN_POINT ( 'NONE',  ( -51.50851365739161736, -25.24728896969645220, 5.995695872060372800 ) ) ;
#81917=FACE_OUTER_BOUND ( 'NONE', #91880, .T. ) ;
#81919=CARTESIAN_POINT ( 'NONE',  ( -104.9228709571500673, -23.47596703998600631, 11.44779298504227860 ) ) ;
#81920=ORIENTED_EDGE ( 'NONE', *, *, #35907, .T. ) ;
#81923=CARTESIAN_POINT ( 'NONE',  ( -75.52287095715007581, -24.15431212366391023, -0.2830839119429213735 ) ) ;
#81925=CARTESIAN_POINT ( 'NONE',  ( -32.99388727629348494, -29.50248914092071928, 2.831113219569932227 ) ) ;
#81926=CARTESIAN_POINT ( 'NONE',  ( -48.62287095715008434, -23.96127896941632329, -0.6493128931037863705 ) ) ;
#81927=FACE_OUTER_BOUND ( 'NONE', #49551, .T. ) ;
#81929=CARTESIAN_POINT ( 'NONE',  ( 8.513215801882951794, -17.43586836189350819, 11.49999999999999645 ) ) ;
#81931=CARTESIAN_POINT ( 'NONE',  ( -15.54266751046811557, -16.22994250641250957, -1.500000000000002220 ) ) ;
#81933=CARTESIAN_POINT ( 'NONE',  ( -101.6235504712075226, -24.66019654487200086, 8.947790411086115725 ) ) ;
#81936=CARTESIAN_POINT ( 'NONE',  ( -63.91063125405472789, -25.14081846633246897, 7.291654623549837844 ) ) ;
#81937=CARTESIAN_POINT ( 'NONE',  ( 19.11985901488480621, -4.296470200863222288, 11.49999999999998934 ) ) ;
#81938=CARTESIAN_POINT ( 'NONE',  ( -119.9228709571500531, -23.47596703998600631, 11.44779298504227860 ) ) ;
#81939=ORIENTED_EDGE ( 'NONE', *, *, #26109, .T. ) ;
#81940=CARTESIAN_POINT ( 'NONE',  ( -21.45671390985790694, -1.711987587955616119, 11.49999999999998934 ) ) ;
#81941=CARTESIAN_POINT ( 'NONE',  ( -125.5228709571500616, -24.99132157543084531, 2.256160258750667502 ) ) ;
#81943=CARTESIAN_POINT ( 'NONE',  ( -100.5228709571500616, -29.50247984919015209, -1.443849546365050029 ) ) ;
#81944=CARTESIAN_POINT ( 'NONE',  ( -99.78454658038423020, -25.27473267031680493, 3.502964407505847699 ) ) ;
#81945=CARTESIAN_POINT ( 'NONE',  ( -7.281717392095591102, 21.80608952751712692, -1.500000000000002220 ) ) ;
#81946=VECTOR ( 'NONE', #15334, 1000.000000000000114 ) ;
#81949=FACE_OUTER_BOUND ( 'NONE', #57354, .T. ) ;
#81951=CARTESIAN_POINT ( 'NONE',  ( -17.93149374516376682, -9.230432107326475233, 11.49999999999999645 ) ) ;
#81952=CARTESIAN_POINT ( 'NONE',  ( -108.9756736452620771, -25.10927630203814331, 3.908685950094584083 ) ) ;
#81953=CARTESIAN_POINT ( 'NONE',  ( -32.65034022602505104, -23.96169478059712787, 10.65365249895719124 ) ) ;
#81954=VECTOR ( 'NONE', #44237, 1000.000000000000114 ) ;
#81958=B_SPLINE_CURVE_WITH_KNOTS ( 'NONE', 3,
 ( #82345, #38156, #69109, #74723, #5225, #36181 ),
 .UNSPECIFIED., .F., .F.,
 ( 4, 2, 4 ),
 ( 0.000000000000000000, 0.001380901958385381606, 0.002761803916770763211 ),
 .UNSPECIFIED. ) ;
#81959=CARTESIAN_POINT ( 'NONE',  ( -126.5895376238167245, -23.48786465467242124, 11.44779295918253403 ) ) ;
#81960=CARTESIAN_POINT ( 'NONE',  ( -13.56193660873917395, -14.51407242162769151, 11.49999999999998934 ) ) ;
#81962=CARTESIAN_POINT ( 'NONE',  ( -47.62287095715004881, -24.66019654487199020, 8.947790411086133489 ) ) ;
#81964=CARTESIAN_POINT ( 'NONE',  ( -10.60818629614422370, 16.63341085705455669, -1.500000000000002220 ) ) ;
#81965=ADVANCED_FACE ( 'NONE', ( #78551 ), #9056, .F. ) ;
#81966=AXIS2_PLACEMENT_3D ( 'NONE', #96978, #90363, #29454 ) ;
#81967=DIRECTION ( 'NONE',  ( -3.773278334453079030E-23, 0.9999999999976377785, 2.173523156925979128E-06 ) ) ;
#81968=ADVANCED_FACE ( 'NONE', ( #80070 ), #69375, .T. ) ;
#81969=EDGE_CURVE ( 'NONE', #9400, #1176, #34398, .T. ) ;
#81971=CARTESIAN_POINT ( 'NONE',  ( -48.62287095715004881, -23.48786465467241058, 11.44779295918254824 ) ) ;
#81972=CARTESIAN_POINT ( 'NONE',  ( -15.36756058500021282, 13.76162614515376426, 11.49999999999999645 ) ) ;
#81973=CARTESIAN_POINT ( 'NONE',  ( -113.6228709571500559, -23.47593901973091235, -1.443836447538999312 ) ) ;
#81975=CARTESIAN_POINT ( 'NONE',  ( -18.74212433040710479, 12.77821124017617649, 11.49999999999999645 ) ) ;
#81976=ORIENTED_EDGE ( 'NONE', *, *, #80151, .F. ) ;
#81979=ADVANCED_FACE ( 'NONE', ( #33895 ), #64881, .T. ) ;
#81981=CARTESIAN_POINT ( 'NONE',  ( -45.62287095715004881, -25.00158670708908915, 2.256160236439166855 ) ) ;
#81985=CARTESIAN_POINT ( 'NONE',  ( -99.61095392075885968, -25.16913655607350009, 6.819335884888137578 ) ) ;
#81986=CARTESIAN_POINT ( 'NONE',  ( 20.41593879258296695, -10.28030303932802880, -1.500000000000002220 ) ) ;
#81987=CARTESIAN_POINT ( 'NONE',  ( -74.62287095715008434, -23.96127896941632685, -0.6493128931037843721 ) ) ;
#81988=CARTESIAN_POINT ( 'NONE',  ( -21.01953065494444317, -4.859126342152997324, -1.500000000000002220 ) ) ;
#81989=CARTESIAN_POINT ( 'NONE',  ( -113.5881221940176005, -24.51419770103157347, 9.386484678747168076 ) ) ;
#81990=CARTESIAN_POINT ( 'NONE',  ( -89.81226385320383088, -25.05712135967894838, 7.447789548357302891 ) ) ;
#81991=CARTESIAN_POINT ( 'NONE',  ( 18.83488669200175281, -12.41447709603701632, 11.49999999999999645 ) ) ;
#81992=ORIENTED_EDGE ( 'NONE', *, *, #24748, .T. ) ;
#81993=CARTESIAN_POINT ( 'NONE',  ( -70.22848692110255797, -25.24754246103700694, 4.852864574778647189 ) ) ;
#81994=B_SPLINE_CURVE_WITH_KNOTS ( 'NONE', 3,
 ( #13462, #66287, #5860, #50542, #5364, #36318, #42449, #67278 ),
 .UNSPECIFIED., .F., .F.,
 ( 4, 2, 2, 4 ),
 ( 6.384118678609026632E-06, 0.002007151183507258855, 0.003007534715921582075, 0.004007918248335905730 ),
 .UNSPECIFIED. ) ;
#81995=CARTESIAN_POINT ( 'NONE',  ( -13.73438224071023761, 17.16576579689093762, -1.500000000000002220 ) ) ;
#81997=CARTESIAN_POINT ( 'NONE',  ( -44.50616043664086163, -23.96169478059713143, 10.65365249895718414 ) ) ;
#82000=LINE ( 'NONE', #97719, #13577 ) ;
#82002=ORIENTED_EDGE ( 'NONE', *, *, #65073, .F. ) ;
#82007=CARTESIAN_POINT ( 'NONE',  ( -110.6228709571500843, -23.47596703998600631, 11.44779298504227860 ) ) ;
#82008=CARTESIAN_POINT ( 'NONE',  ( -104.5228709571501327, -23.96127896941634106, -0.6493128931037958074 ) ) ;
#82009=CARTESIAN_POINT ( 'NONE',  ( -57.48876574585108301, -24.65952944569304606, 1.056160979905698571 ) ) ;
#82010=CARTESIAN_POINT ( 'NONE',  ( 18.82465703714932204, -7.861812626244089053, -1.500000000000002220 ) ) ;
#82012=DIRECTION ( 'NONE',  ( 0.000000000000000000, 0.9999999999976377785, 2.173523156925979128E-06 ) ) ;
#82016=CARTESIAN_POINT ( 'NONE',  ( -35.58953762381672448, -23.47593901973091235, -1.443836447539011525 ) ) ;
#82019=CARTESIAN_POINT ( 'NONE',  ( -33.62287095715005592, -24.65952944569304250, 1.056160979905690356 ) ) ;
#82020=ORIENTED_EDGE ( 'NONE', *, *, #36031, .T. ) ;
#82021=CARTESIAN_POINT ( 'NONE',  ( 8.872108392497455753, -18.76566404461018678, 11.49999999999998934 ) ) ;
#82022=EDGE_CURVE ( 'NONE', #85000, #41774, #26783, .T. ) ;
#82025=EDGE_LOOP ( 'NONE', ( #77886, #59493, #91356, #14017 ) ) ;
#82027=FACE_OUTER_BOUND ( 'NONE', #57896, .T. ) ;
#82030=EDGE_LOOP ( 'NONE', ( #15050, #82514, #34008, #8969 ) ) ;
#82031=AXIS2_PLACEMENT_3D ( 'NONE', #87002, #86502, #40828 ) ;
#82032=CARTESIAN_POINT ( 'NONE',  ( -79.55620429048339304, -24.65952944569304961, 1.056160979905700348 ) ) ;
#82033=DIRECTION ( 'NONE',  ( 0.000000000000000000, -2.173523156925980399E-06, 0.9999999999976378895 ) ) ;
#82036=CARTESIAN_POINT ( 'NONE',  ( -71.29000553066028090, -25.31201746252870421, 6.029836970080467040 ) ) ;
#82037=CARTESIAN_POINT ( 'NONE',  ( 1.153593019990587942, -22.03401787307112869, 11.49999999999999645 ) ) ;
#82040=DIRECTION ( 'NONE',  ( 0.000000000000000000, -2.173523156925979552E-06, 0.9999999999976378895 ) ) ;
#82041=CARTESIAN_POINT ( 'NONE',  ( -21.41681981171885951, -7.298096547245328303, -1.500000000000002220 ) ) ;
#82043=CARTESIAN_POINT ( 'NONE',  ( -115.6270093773762397, -24.40133493613050675, 9.663955038902797057 ) ) ;
#82044=ORIENTED_EDGE ( 'NONE', *, *, #26200, .T. ) ;
#82046=CARTESIAN_POINT ( 'NONE',  ( -78.62287095715007013, -24.66019654487199375, 8.947790411086124607 ) ) ;
#82047=CARTESIAN_POINT ( 'NONE',  ( -57.55991801598921853, -23.73791477778911840, 11.05961554403170588 ) ) ;
#82048=ORIENTED_EDGE ( 'NONE', *, *, #4640, .T. ) ;
#82049=CARTESIAN_POINT ( 'NONE',  ( -20.37118330240554087, -5.769015352940915164, -1.500000000000002220 ) ) ;
#82050=B_SPLINE_CURVE_WITH_KNOTS ( 'NONE', 3,
 ( #83833, #100032, #51902, #14808, #84324, #21419 ),
 .UNSPECIFIED., .F., .F.,
 ( 4, 2, 4 ),
 ( 6.384118678609746610E-06, 0.001386860460828373250, 0.002767336802978136688 ),
 .UNSPECIFIED. ) ;
#82051=CARTESIAN_POINT ( 'NONE',  ( -103.5895376238167245, -24.64965694238575011, 8.947790433994194714 ) ) ;
#82052=CARTESIAN_POINT ( 'NONE',  ( 0.6114060112162268412, -22.25658958135186793, -1.500000000000002220 ) ) ;
#82053=B_SPLINE_CURVE_WITH_KNOTS ( 'NONE', 3,
 ( #37240, #38724, #46344, #83401 ),
 .UNSPECIFIED., .F., .F.,
 ( 4, 4 ),
 ( 0.6009291087672576914, 0.6099355400393732252 ),
 .UNSPECIFIED. ) ;
#82054=CARTESIAN_POINT ( 'NONE',  ( -46.62287095715006302, -23.94994826722515313, -0.6494450866351717533 ) ) ;
#82055=VERTEX_POINT ( 'NONE', #43016 ) ;
#82056=CARTESIAN_POINT ( 'NONE',  ( -74.52287095715007581, -23.47596703998600631, 11.44779298504228748 ) ) ;
#82058=VECTOR ( 'NONE', #66008, 1000.000000000000114 ) ;
#82059=DIRECTION ( 'NONE',  ( -3.773278334453079030E-23, 0.9999999999976377785, 2.173523156925979128E-06 ) ) ;
#82060=CARTESIAN_POINT ( 'NONE',  ( -116.5562042904834072, -24.64898659630528854, 1.056161002820835249 ) ) ;
#82061=CARTESIAN_POINT ( 'NONE',  ( 9.662506626059768067, -16.94115208737379774, 11.49999999999998934 ) ) ;
#82062=CARTESIAN_POINT ( 'NONE',  ( 18.29419249859179786, 11.19154738541161365, -1.500000000000002220 ) ) ;
#82063=CARTESIAN_POINT ( 'NONE',  ( -26.72449842520168062, -24.92774724699053124, 1.897193310600636007 ) ) ;
#82065=DIRECTION ( 'NONE',  ( 1.000000000000000000, 3.773278334444167608E-23, 8.201307833595939069E-29 ) ) ;
#82066=CARTESIAN_POINT ( 'NONE',  ( -0.9063223138645676302, -22.79912562917415997, -1.500000000000002220 ) ) ;
#82068=CARTESIAN_POINT ( 'NONE',  ( -106.5926167309080768, -23.96169478059714564, 10.65365249895717170 ) ) ;
#82069=LINE ( 'NONE', #42031, #68674 ) ;
#82070=CARTESIAN_POINT ( 'NONE',  ( 19.87125486832220744, 0.9792442318621276121, 11.49999999999999645 ) ) ;
#82071=CARTESIAN_POINT ( 'NONE',  ( -104.6286256937127206, -24.15543982623907482, -0.2315651400026580709 ) ) ;
#82072=EDGE_CURVE ( 'NONE', #68025, #78274, #87354, .T. ) ;
#82073=B_SPLINE_CURVE_WITH_KNOTS ( 'NONE', 3,
 ( #7599, #77100, #47176, #87222 ),
 .UNSPECIFIED., .F., .F.,
 ( 4, 4 ),
 ( 0.000000000000000000, 9.999999999998897304E-05 ),
 .UNSPECIFIED. ) ;
#82077=VERTEX_POINT ( 'NONE', #20651 ) ;
#82078=CARTESIAN_POINT ( 'NONE',  ( -25.67538399529471249, -24.84156714063196958, 3.473377010405353182 ) ) ;
#82080=EDGE_CURVE ( 'NONE', #38937, #80860, #58242, .T. ) ;
#82081=CARTESIAN_POINT ( 'NONE',  ( -13.51661872714272405, -17.00040112538478709, 11.49999999999998934 ) ) ;
#82083=CARTESIAN_POINT ( 'NONE',  ( -13.79594968651775666, -13.80015156857029268, -1.500000000000002220 ) ) ;
#82084=ADVANCED_FACE ( 'NONE', ( #4455 ), #19656, .F. ) ;
#82086=LINE ( 'NONE', #59760, #65309 ) ;
#82090=CARTESIAN_POINT ( 'NONE',  ( -15.03541999946025243, -13.88573836563254460, 11.49999999999999645 ) ) ;
#82092=AXIS2_PLACEMENT_3D ( 'NONE', #73129, #65537, #64542 ) ;
#82093=CARTESIAN_POINT ( 'NONE',  ( -86.62287095715004170, -24.64965695001468404, 8.947790433994180503 ) ) ;
#82094=ADVANCED_FACE ( 'NONE', ( #35889 ), #65872, .T. ) ;
#82096=CARTESIAN_POINT ( 'NONE',  ( -28.62287095715004881, -24.49675894734168580, 8.947790415257339092 ) ) ;
#82099=DIRECTION ( 'NONE',  ( -3.773278334453079030E-23, 0.9999999999976377785, 2.173523156925979128E-06 ) ) ;
#82100=VECTOR ( 'NONE', #56573, 1000.000000000000114 ) ;
#82102=ORIENTED_EDGE ( 'NONE', *, *, #4947, .F. ) ;
#82105=CARTESIAN_POINT ( 'NONE',  ( -23.02147672596084149, 0.6323230698326208765, 11.49999999999999645 ) ) ;
#82106=CARTESIAN_POINT ( 'NONE',  ( -9.359374538088376383, 20.77767741201286711, 11.49999999999998934 ) ) ;
#82107=CARTESIAN_POINT ( 'NONE',  ( -110.6300949696500453, -24.15602025860899360, 10.28564288303534724 ) ) ;
#82109=PLANE ( 'NONE',  #9562 ) ;
#82111=CARTESIAN_POINT ( 'NONE',  ( -110.5150772214216914, -24.40034930558991633, 0.3402023900116072364 ) ) ;
#82112=CARTESIAN_POINT ( 'NONE',  ( 1.548332177993611225, -21.85883989728069565, -1.500000000000002220 ) ) ;
#82113=CARTESIAN_POINT ( 'NONE',  ( -46.62287095715004881, -29.50250243563736774, 8.947779886222146928 ) ) ;
#82114=DIRECTION ( 'NONE',  ( 0.000000000000000000, -2.173523156925980399E-06, 0.9999999999976378895 ) ) ;
#82117=ORIENTED_EDGE ( 'NONE', *, *, #31383, .T. ) ;
#82118=CARTESIAN_POINT ( 'NONE',  ( 17.38039551199336685, -10.77953091123627694, -1.500000000000002220 ) ) ;
#82120=EDGE_LOOP ( 'NONE', ( #2389, #14837, #92613, #35088 ) ) ;
#82121=VERTEX_POINT ( 'NONE', #96296 ) ;
#82123=CARTESIAN_POINT ( 'NONE',  ( 20.16173082093541424, 11.17373015621797627, 11.49999999999998934 ) ) ;
#82124=CARTESIAN_POINT ( 'NONE',  ( -80.52287095715006160, -24.83602698348159876, 1.605859176311265291 ) ) ;
#82125=CARTESIAN_POINT ( 'NONE',  ( 5.465678960246475704, -19.50585317057041124, -1.500000000000002220 ) ) ;
#82126=ORIENTED_EDGE ( 'NONE', *, *, #18605, .F. ) ;
#82127=AXIS2_PLACEMENT_3D ( 'NONE', #69903, #37460, #53192 ) ;
#82128=CARTESIAN_POINT ( 'NONE',  ( -69.62287095715005592, -23.47596703998600631, 11.44779298504227683 ) ) ;
#82129=CARTESIAN_POINT ( 'NONE',  ( -49.62287095715005592, -23.47593901973091235, -1.443836447539009749 ) ) ;
#82130=CARTESIAN_POINT ( 'NONE',  ( -95.62359478722041217, -25.00158670708911046, 2.256160236439221034 ) ) ;
#82131=CARTESIAN_POINT ( 'NONE',  ( -53.59317311883835089, -24.15620529776627734, 10.23563542870660825 ) ) ;
#82132=CARTESIAN_POINT ( 'NONE',  ( -5.188002292566340934, -20.72503599944539587, 11.49999999999999645 ) ) ;
#82133=ORIENTED_EDGE ( 'NONE', *, *, #34197, .T. ) ;
#82137=CARTESIAN_POINT ( 'NONE',  ( 22.02009960291501045, 3.200778107580485532, -1.500000000000002220 ) ) ;
#82138=CARTESIAN_POINT ( 'NONE',  ( -10.41657757243416604, 17.86655067824183618, 11.49999999999998934 ) ) ;
#82142=ORIENTED_EDGE ( 'NONE', *, *, #73888, .T. ) ;
#82143=CARTESIAN_POINT ( 'NONE',  ( -61.55620429048339304, -24.66019654487199020, 8.947790411086131712 ) ) ;
#82144=EDGE_LOOP ( 'NONE', ( #96822, #42398, #76400, #83099 ) ) ;
#82145=CARTESIAN_POINT ( 'NONE',  ( 20.69369447470243628, -3.267675865747468489, -1.500000000000002220 ) ) ;
#82146=CARTESIAN_POINT ( 'NONE',  ( -19.93956527825925917, 9.129326121205059152, 11.49999999999999645 ) ) ;
#82148=CARTESIAN_POINT ( 'NONE',  ( -18.95691745938505335, -12.16397891629814865, 11.49999999999998934 ) ) ;
#82150=CARTESIAN_POINT ( 'NONE',  ( 17.15856466979341377, 12.00972951212132855, -1.500000000000002220 ) ) ;
#82151=CARTESIAN_POINT ( 'NONE',  ( -92.64087933133858144, -23.48786465467241058, 11.44779295918254469 ) ) ;
#82158=CARTESIAN_POINT ( 'NONE',  ( -66.54418166932423162, -24.34968618360933235, 0.1864209137778773950 ) ) ;
#82160=CARTESIAN_POINT ( 'NONE',  ( -20.86232423683148340, -5.086641213604358391, -1.500000000000002220 ) ) ;
#82161=CARTESIAN_POINT ( 'NONE',  ( -80.62287095715005592, -29.50247984919015209, -1.443849546365053582 ) ) ;
#82164=CARTESIAN_POINT ( 'NONE',  ( -11.11193726737652199, 17.91617163517716804, 11.49999999999998934 ) ) ;
#82167=CARTESIAN_POINT ( 'NONE',  ( -50.48970033773105115, -24.52399227489126687, 9.353111116836522854 ) ) ;
#82168=AXIS2_PLACEMENT_3D ( 'NONE', #96507, #41745, #42255 ) ;
#82170=PLANE ( 'NONE',  #69757 ) ;
#82171=CARTESIAN_POINT ( 'NONE',  ( 21.00647827173414939, 6.864759178008983831, -1.500000000000002220 ) ) ;
#82176=FACE_OUTER_BOUND ( 'NONE', #25337, .T. ) ;
#82177=CARTESIAN_POINT ( 'NONE',  ( 12.02608574658498597, -17.65016651952024063, -1.500000000000002220 ) ) ;
#82178=CARTESIAN_POINT ( 'NONE',  ( -66.52287095715006160, -23.48783264082476663, -1.443836473390092134 ) ) ;
#82179=FACE_BOUND ( 'NONE', #94722, .T. ) ;
#82180=CARTESIAN_POINT ( 'NONE',  ( -86.55620429048336462, -24.64898659630528854, 1.056161002820825923 ) ) ;
#82182=CARTESIAN_POINT ( 'NONE',  ( 3.115699594417459473, -22.39947108414558485, -1.500000000000002220 ) ) ;
#82184=CARTESIAN_POINT ( 'NONE',  ( -109.5228709571500474, -24.66019654487200086, 8.947790411086119278 ) ) ;
#82185=DIRECTION ( 'NONE',  ( 1.000000000000000000, 3.773278334444166432E-23, 8.201307841325785021E-29 ) ) ;
#82186=CARTESIAN_POINT ( 'NONE',  ( -19.76903914530799966, 0.2396048511829373395, 11.49999999999999645 ) ) ;
#82189=CARTESIAN_POINT ( 'NONE',  ( -67.49335235930752219, -24.65952944569304606, 1.056160979905700570 ) ) ;
#82190=ORIENTED_EDGE ( 'NONE', *, *, #12897, .T. ) ;
#82192=CARTESIAN_POINT ( 'NONE',  ( -29.71166344112055668, -24.60094320703244364, 3.608441551108168444 ) ) ;
#82193=EDGE_CURVE ( 'NONE', #35568, #14950, #5054, .T. ) ;
#82195=CARTESIAN_POINT ( 'NONE',  ( 15.46703529437019853, -15.08741104398349187, 11.49999999999998934 ) ) ;
#82197=CARTESIAN_POINT ( 'NONE',  ( -49.88732701573676565, -25.10935145987042105, 2.919595231271752134 ) ) ;
#82198=CARTESIAN_POINT ( 'NONE',  ( -18.68205546197936684, -5.105407162728520021, -1.500000000000002220 ) ) ;
#82199=EDGE_CURVE ( 'NONE', #86774, #20204, #7426, .T. ) ;
#82202=CARTESIAN_POINT ( 'NONE',  ( -17.91562471463183570, -8.470225615102204841, 11.49999999999998934 ) ) ;
#82203=ORIENTED_EDGE ( 'NONE', *, *, #93765, .T. ) ;
#82204=ADVANCED_FACE ( 'NONE', ( #38379 ), #43998, .F. ) ;
#82205=CARTESIAN_POINT ( 'NONE',  ( 12.36038202409810438, -16.04522380935875248, 11.49999999999999645 ) ) ;
#82207=EDGE_CURVE ( 'NONE', #44485, #59914, #46208, .T. ) ;
#82209=ORIENTED_EDGE ( 'NONE', *, *, #58212, .F. ) ;
#82211=CARTESIAN_POINT ( 'NONE',  ( -102.6228709571500275, -23.48783264082478794, -1.443836473390062158 ) ) ;
#82214=DIRECTION ( 'NONE',  ( -3.773278334453079030E-23, 0.9999999999976377785, 2.173523156925979128E-06 ) ) ;
#82215=CARTESIAN_POINT ( 'NONE',  ( -1.415466703587968667, 19.98303252902060834, -1.500000000000002220 ) ) ;
#82216=ADVANCED_FACE ( 'NONE', ( #29272 ), #45014, .T. ) ;
#82218=ORIENTED_EDGE ( 'NONE', *, *, #24340, .F. ) ;
#82223=CARTESIAN_POINT ( 'NONE',  ( -113.5228709571500616, -23.72747288104470087, -1.053458166803225238 ) ) ;
#82227=VERTEX_POINT ( 'NONE', #53628 ) ;
#82229=CARTESIAN_POINT ( 'NONE',  ( 13.61570878652767291, 15.11107311891478666, -1.500000000000002220 ) ) ;
#82231=EDGE_CURVE ( 'NONE', #88368, #98147, #83552, .T. ) ;
#82232=CARTESIAN_POINT ( 'NONE',  ( 21.75294195941402364, -7.338126679257295670, 11.49999999999998934 ) ) ;
#82234=ORIENTED_EDGE ( 'NONE', *, *, #12563, .T. ) ;
#82235=CARTESIAN_POINT ( 'NONE',  ( -89.62287095715002749, -23.48783264082478439, -1.443836473390063713 ) ) ;
#82236=CARTESIAN_POINT ( 'NONE',  ( -49.44941220326682441, -25.12215325162356905, 6.666982529036616256 ) ) ;
#82237=EDGE_CURVE ( 'NONE', #65949, #52778, #91169, .T. ) ;
#82238=CARTESIAN_POINT ( 'NONE',  ( -125.6228709571500559, -29.50248789122583659, 2.256150453626215580 ) ) ;
#82239=CARTESIAN_POINT ( 'NONE',  ( 16.79009078985406234, 12.93418496121567252, 11.49999999999999645 ) ) ;
#82240=ORIENTED_EDGE ( 'NONE', *, *, #4546, .T. ) ;
#82241=EDGE_LOOP ( 'NONE', ( #64061, #32070, #36258, #32864 ) ) ;
#82242=CARTESIAN_POINT ( 'NONE',  ( -0.8124730928778809425, -22.15030348749839817, -1.500000000000002220 ) ) ;
#82243=CARTESIAN_POINT ( 'NONE',  ( 17.30552477474510908, -11.17933342135444086, -1.500000000000002220 ) ) ;
#82245=ORIENTED_EDGE ( 'NONE', *, *, #23512, .T. ) ;
#82246=DIRECTION ( 'NONE',  ( -3.773278334453079618E-23, 0.9999999999976377785, 2.173523156925979975E-06 ) ) ;
#82247=ADVANCED_FACE ( 'NONE', ( #23137 ), #45513, .F. ) ;
#82248=CARTESIAN_POINT ( 'NONE',  ( -87.62287095715004170, -29.50248528299804818, 1.056150453629040253 ) ) ;
#82249=ORIENTED_EDGE ( 'NONE', *, *, #34085, .F. ) ;
#82250=VERTEX_POINT ( 'NONE', #44506 ) ;
#82254=CARTESIAN_POINT ( 'NONE',  ( -49.52287095715006160, -24.64965694238406613, 8.947790433994203596 ) ) ;
#82255=CARTESIAN_POINT ( 'NONE',  ( -28.52198423978972741, -23.32371265842308716, 11.44779300624184160 ) ) ;
#82256=CARTESIAN_POINT ( 'NONE',  ( -119.6228709571500559, -23.48783264082479150, -1.443836473390058384 ) ) ;
#82257=CARTESIAN_POINT ( 'NONE',  ( -12.88759680649768136, 16.30154091734715749, -1.500000000000002220 ) ) ;
#82258=CARTESIAN_POINT ( 'NONE',  ( -18.02536786162489335, -12.12045427182966861, 11.49999999999999645 ) ) ;
#82261=CARTESIAN_POINT ( 'NONE',  ( -51.93149462243456327, -25.24900417239232908, 6.174051150523328424 ) ) ;
#82264=CARTESIAN_POINT ( 'NONE',  ( -115.5168712054073410, -24.40034930558990567, 0.3402023900116066257 ) ) ;
#82265=CARTESIAN_POINT ( 'NONE',  ( -19.61019785865472542, -10.87575402790796453, 11.49999999999998934 ) ) ;
#82266=CARTESIAN_POINT ( 'NONE',  ( -50.56373716527822637, -25.31296762218556395, 4.723080049254409829 ) ) ;
#82269=CARTESIAN_POINT ( 'NONE',  ( -75.52287095715006160, -23.84047902841601285, -0.8780736468305737619 ) ) ;
#82271=B_SPLINE_CURVE_WITH_KNOTS ( 'NONE', 3,
 ( #95694, #87077, #79463, #82332, #50898, #9955 ),
 .UNSPECIFIED., .F., .F.,
 ( 4, 2, 4 ),
 ( 6.391158118955278476E-06, 0.001387004593080777256, 0.002767618028042598960 ),
 .UNSPECIFIED. ) ;
#82272=B_SPLINE_SURFACE_WITH_KNOTS ( 'NONE', 3, 3, ( 
 ( #44084, #45590, #98854, #92246 ),
 ( #51699, #82632, #60321, #91248 ),
 ( #45091, #90255, #97854, #21721 ),
 ( #52695, #68915, #84635, #36462 ),
 ( #6519, #37471, #98352, #5018 ),
 ( #83634, #14116, #29850, #22717 ),
 ( #60821, #74526, #20730, #67427 ) ),
 .UNSPECIFIED., .F., .F., .F.,
 ( 4, 3, 4 ),
 ( 4, 4 ),
 ( 0.0004767420375739903028, 0.1029714262224254440, 0.2054661104072768862 ),
 ( 0.06486343431056791620, 0.06976593829091715104 ),
 .UNSPECIFIED. ) ;
#82274=ORIENTED_EDGE ( 'NONE', *, *, #18217, .T. ) ;
#82277=ORIENTED_EDGE ( 'NONE', *, *, #9814, .T. ) ;
#82278=CARTESIAN_POINT ( 'NONE',  ( 14.64190796094839264, -15.47823801613018269, -1.500000000000002220 ) ) ;
#82279=ORIENTED_EDGE ( 'NONE', *, *, #6844, .T. ) ;
#82280=CARTESIAN_POINT ( 'NONE',  ( -58.62287095715004881, -24.64898659630367916, 1.056161002820822592 ) ) ;
#82281=CARTESIAN_POINT ( 'NONE',  ( 19.20967809413044236, -10.42350525531561978, -1.500000000000002220 ) ) ;
#82282=CARTESIAN_POINT ( 'NONE',  ( -124.5562042904833930, -23.47596703998600631, 11.44779298504227683 ) ) ;
#82283=CARTESIAN_POINT ( 'NONE',  ( 2.290073164716609710, 22.57640404599860418, -1.500000000000002220 ) ) ;
#82284=DIRECTION ( 'NONE',  ( -3.773278334453079618E-23, 0.9999999999976377785, 2.173523156925979975E-06 ) ) ;
#82286=CARTESIAN_POINT ( 'NONE',  ( 18.32745805453730981, -11.99952526121574259, -1.500000000000002220 ) ) ;
#82288=ORIENTED_EDGE ( 'NONE', *, *, #52422, .F. ) ;
#82289=CARTESIAN_POINT ( 'NONE',  ( -122.5913845940917213, -23.73791477778912551, 11.05961554403169878 ) ) ;
#82293=CARTESIAN_POINT ( 'NONE',  ( -105.5228709571500758, -29.50250243563736774, 8.947779886222136270 ) ) ;
#82295=CARTESIAN_POINT ( 'NONE',  ( -0.07188169300783608939, -22.11943499646449141, 0.5637492489085879077 ) ) ;
#82296=CARTESIAN_POINT ( 'NONE',  ( -21.25539211000977957, 0.9166567589900279645, 11.49999999999998934 ) ) ;
#82297=CARTESIAN_POINT ( 'NONE',  ( -55.62287095715007013, -24.92604778743017491, 8.074972756849359001 ) ) ;
#82298=CARTESIAN_POINT ( 'NONE',  ( -26.21213932664330670, -24.97064719818860468, 3.737063582475403933 ) ) ;
#82299=CARTESIAN_POINT ( 'NONE',  ( -85.63840790987890728, -24.15503026093914229, -0.2815557561904377115 ) ) ;
#82301=FACE_OUTER_BOUND ( 'NONE', #87402, .T. ) ;
#82304=CARTESIAN_POINT ( 'NONE',  ( 6.866622826037362515, -18.30913693658520103, 11.49999999999999645 ) ) ;
#82305=CARTESIAN_POINT ( 'NONE',  ( -58.62287095715004881, -23.48786465467241769, 11.44779295918254824 ) ) ;
#82311=CARTESIAN_POINT ( 'NONE',  ( -99.46521863968663979, -25.31559379708168223, 5.025132061053519728 ) ) ;
#82312=CARTESIAN_POINT ( 'NONE',  ( -31.62287095715005236, -24.50216790748098461, 0.6166512839513674793 ) ) ;
#82313=CARTESIAN_POINT ( 'NONE',  ( -40.62287095715004170, -24.99156045073392463, 7.747789690856161648 ) ) ;
#82314=CARTESIAN_POINT ( 'NONE',  ( 14.14096853472169535, -13.71769858867784464, -1.500000000000002220 ) ) ;
#82316=ORIENTED_EDGE ( 'NONE', *, *, #85917, .T. ) ;
#82322=ORIENTED_EDGE ( 'NONE', *, *, #64753, .T. ) ;
#82324=CARTESIAN_POINT ( 'NONE',  ( -45.62287095715004881, -24.52323809116984421, 9.355190652339420154 ) ) ;
#82325=CARTESIAN_POINT ( 'NONE',  ( -55.64837685101972653, -24.15503026093915295, -0.2815557561904505901 ) ) ;
#82326=DIRECTION ( 'NONE',  ( 1.000000000000000000, 3.773278334444166432E-23, 8.201307841325785021E-29 ) ) ;
#82327=CARTESIAN_POINT ( 'NONE',  ( -31.62287095715005236, -23.72773821059535493, 11.05748984161097503 ) ) ;
#82328=CARTESIAN_POINT ( 'NONE',  ( -32.07722060962682775, -24.86441978397624553, 8.247789967200544581 ) ) ;
#82329=CARTESIAN_POINT ( 'NONE',  ( -107.6262949015405042, -24.34968618360934300, 0.1864209137778969627 ) ) ;
#82330=CARTESIAN_POINT ( 'NONE',  ( 18.23660095519748481, -8.086948576924280374, -1.500000000000002220 ) ) ;
#82331=EDGE_CURVE ( 'NONE', #99388, #63165, #28776, .T. ) ;
#82332=CARTESIAN_POINT ( 'NONE',  ( -54.52287095715005449, -24.35013146730203815, 9.818937971375104823 ) ) ;
#82333=CARTESIAN_POINT ( 'NONE',  ( -0.001635060676233153704, -23.02883285463877527, 4.281990464225436277 ) ) ;
#82338=CARTESIAN_POINT ( 'NONE',  ( -80.50190673274472886, -24.52399227489127043, 9.353111116836524630 ) ) ;
#82340=CARTESIAN_POINT ( 'NONE',  ( -39.56973724660041825, -23.48783264082476308, -1.443836473390098352 ) ) ;
#82341=CARTESIAN_POINT ( 'NONE',  ( -64.52287095715006160, -24.51283580621364422, 0.6167428607019732612 ) ) ;
#82342=FACE_OUTER_BOUND ( 'NONE', #67385, .T. ) ;
#82343=ORIENTED_EDGE ( 'NONE', *, *, #1754, .T. ) ;
#82345=CARTESIAN_POINT ( 'NONE',  ( -37.62287095715007013, -23.47596703998600276, 11.44779298504227505 ) ) ;
#82346=PLANE ( 'NONE',  #37095 ) ;
#82348=CARTESIAN_POINT ( 'NONE',  ( 8.147030896810244727, 18.52525024547675869, -1.500000000000002220 ) ) ;
#82352=CARTESIAN_POINT ( 'NONE',  ( -82.62287095715007013, -24.66019654487199375, 8.947790411086128159 ) ) ;
#82354=CARTESIAN_POINT ( 'NONE',  ( -106.5228709571500758, -23.47596703998600631, 11.44779298504228038 ) ) ;
#82357=CARTESIAN_POINT ( 'NONE',  ( 15.05167116458888010, 13.23127732593390959, -1.500000000000002220 ) ) ;
#82358=CARTESIAN_POINT ( 'NONE',  ( 15.37114825158464271, 14.37155165002682544, 11.49999999999999645 ) ) ;
#82359=DIRECTION ( 'NONE',  ( -3.773278334453079618E-23, 0.9999999999976377785, 2.173523156925979975E-06 ) ) ;
#82360=CARTESIAN_POINT ( 'NONE',  ( -32.52287095715006160, -23.48783264083359867, -1.443836473376375329 ) ) ;
#82361=CARTESIAN_POINT ( 'NONE',  ( -19.90388773112789167, 9.559999800501117306, 11.49999999999998934 ) ) ;
#82363=CARTESIAN_POINT ( 'NONE',  ( -66.58953762381673869, -24.66019654487198665, 8.947790411086131712 ) ) ;
#82365=CARTESIAN_POINT ( 'NONE',  ( -87.52287095715006160, -24.65952944569304606, 1.056160979905700570 ) ) ;
#82366=CARTESIAN_POINT ( 'NONE',  ( -118.5562042904833930, -24.64898659630529565, 1.056161002820835026 ) ) ;
#82367=ORIENTED_EDGE ( 'NONE', *, *, #36637, .F. ) ;
#82368=CARTESIAN_POINT ( 'NONE',  ( -89.40841769935764205, -25.30749613935913089, 3.864043853429952158 ) ) ;
#82369=CARTESIAN_POINT ( 'NONE',  ( -31.51236532535822832, -23.73766607897669800, -1.055555164236445131 ) ) ;
#82370=ORIENTED_EDGE ( 'NONE', *, *, #28808, .F. ) ;
#82372=ORIENTED_EDGE ( 'NONE', *, *, #55562, .T. ) ;
#82375=FACE_OUTER_BOUND ( 'NONE', #16355, .T. ) ;
#82376=CARTESIAN_POINT ( 'NONE',  ( -20.42507745660439156, -2.452541965221147535, -1.500000000000002220 ) ) ;
#82377=CARTESIAN_POINT ( 'NONE',  ( -15.49073194614445015, 15.02706685249526686, 11.49999999999999645 ) ) ;
#82378=ORIENTED_EDGE ( 'NONE', *, *, #32774, .F. ) ;
#82379=CARTESIAN_POINT ( 'NONE',  ( -91.52216445584937787, -23.48783264082477018, -1.443836473390090802 ) ) ;
#82380=CARTESIAN_POINT ( 'NONE',  ( -99.21406825799371632, -25.29348853684751575, 4.454428177689103485 ) ) ;
#82382=CARTESIAN_POINT ( 'NONE',  ( 14.50327815619135308, -17.01817589256642194, 11.49999999999998934 ) ) ;
#82384=CARTESIAN_POINT ( 'NONE',  ( -82.58953762381672448, -23.47593901973091235, -1.443836447539004642 ) ) ;
#82385=ORIENTED_EDGE ( 'NONE', *, *, #65397, .T. ) ;
#82386=CARTESIAN_POINT ( 'NONE',  ( -50.62287095715005592, -25.00182538069145011, 7.747789668545097541 ) ) ;
#82387=CARTESIAN_POINT ( 'NONE',  ( -96.52287095715006160, -23.48786465467241769, 11.44779295918254114 ) ) ;
#82388=CARTESIAN_POINT ( 'NONE',  ( -13.97254113366623152, 15.51630364309664856, 11.49999999999998934 ) ) ;
#82391=CARTESIAN_POINT ( 'NONE',  ( -39.05155750314200702, -25.26703200855950016, 4.030863154173684570 ) ) ;
#82393=VERTEX_POINT ( 'NONE', #54615 ) ;
#82394=CARTESIAN_POINT ( 'NONE',  ( -100.6278523261951676, -24.63419186844610920, 9.035850630976920428 ) ) ;
#82395=CARTESIAN_POINT ( 'NONE',  ( 14.48694714638828884, 15.39972936300609341, -1.500000000000002220 ) ) ;
#82396=ORIENTED_EDGE ( 'NONE', *, *, #5274, .F. ) ;
#82397=CARTESIAN_POINT ( 'NONE',  ( -117.6250645124119103, -24.34968618360934656, 0.1864209137778901626 ) ) ;
#82398=CARTESIAN_POINT ( 'NONE',  ( -98.55620429048337883, -23.48783264082478084, -1.443836473390061936 ) ) ;
#82399=CARTESIAN_POINT ( 'NONE',  ( -129.5562042904834072, -23.48786465467241413, 11.44779295918253581 ) ) ;
#82402=CARTESIAN_POINT ( 'NONE',  ( -16.45766974254678061, 14.19212061201335473, -1.500000000000002220 ) ) ;
#82403=CARTESIAN_POINT ( 'NONE',  ( -80.30325611392450469, -25.04485593722630554, 7.554940489935124681 ) ) ;
#82404=CARTESIAN_POINT ( 'NONE',  ( -5.491053050139323766, 21.65304554001118120, 11.49999999999999645 ) ) ;
#82405=ORIENTED_EDGE ( 'NONE', *, *, #25652, .F. ) ;
#82406=DIRECTION ( 'NONE',  ( -3.773278334453079618E-23, 0.9999999999976377785, 2.173523156925979975E-06 ) ) ;
#82407=CARTESIAN_POINT ( 'NONE',  ( -95.58953762381673869, -23.48786465467241769, 11.44779295918254114 ) ) ;
#82408=CARTESIAN_POINT ( 'NONE',  ( -31.62287095715005236, -24.64898659630367206, 1.056161002820817485 ) ) ;
#82413=EDGE_LOOP ( 'NONE', ( #98948, #23215, #79854, #41962 ) ) ;
#82414=CARTESIAN_POINT ( 'NONE',  ( -33.62287095715005592, -23.47593901973091235, -1.443836447539013301 ) ) ;
#82415=DIRECTION ( 'NONE',  ( -3.773278334453079030E-23, 0.9999999999976377785, 2.173523156925979128E-06 ) ) ;
#82417=CARTESIAN_POINT ( 'NONE',  ( -43.62287095715004170, -23.95044443724992078, 10.65354141964649948 ) ) ;
#82421=CARTESIAN_POINT ( 'NONE',  ( -8.550378450311910683, 17.38971893761031851, 11.49999999999999645 ) ) ;
#82430=CARTESIAN_POINT ( 'NONE',  ( -36.52287095715006870, -23.48786465467240347, 11.44779295918255180 ) ) ;
#82431=CARTESIAN_POINT ( 'NONE',  ( 18.62133539762988121, 6.091496293051981148, -1.500000000000002220 ) ) ;
#82434=CARTESIAN_POINT ( 'NONE',  ( 8.794441374123232791, -19.68457759291379716, 11.49999999999998934 ) ) ;
#82436=CARTESIAN_POINT ( 'NONE',  ( -33.65006591098492805, -23.96169478059712432, 10.65365249895719124 ) ) ;
#82437=CARTESIAN_POINT ( 'NONE',  ( -70.42265764498320380, -25.25639600851986089, 7.098707395884841453 ) ) ;
#82438=CARTESIAN_POINT ( 'NONE',  ( -40.50924942470576440, -23.85016227208580730, -0.8807180028928395243 ) ) ;
#82439=CARTESIAN_POINT ( 'NONE',  ( -100.1584806888234738, -25.18439341914872287, 3.322325955448823365 ) ) ;
#82440=CARTESIAN_POINT ( 'NONE',  ( -1.485350438481424895, -22.96994831426971828, -1.500000000000002220 ) ) ;
#82442=EDGE_CURVE ( 'NONE', #25123, #88484, #79986, .T. ) ;
#82446=CARTESIAN_POINT ( 'NONE',  ( 1.915021276000606454, 20.04344799065331628, 11.49999999999999645 ) ) ;
#82447=CARTESIAN_POINT ( 'NONE',  ( -92.62287095715005592, -23.47596703998600631, 11.44779298504227860 ) ) ;
#82448=CARTESIAN_POINT ( 'NONE',  ( -36.62287095715005592, -29.50248528299804818, 1.056150453629031594 ) ) ;
#82450=CARTESIAN_POINT ( 'NONE',  ( -94.62287095715005592, -23.48786465467241769, 11.44779295918254114 ) ) ;
#82452=CARTESIAN_POINT ( 'NONE',  ( -111.0533842133887390, -25.29779214506538310, 3.566049847669544359 ) ) ;
#82453=CARTESIAN_POINT ( 'NONE',  ( 10.41257876278241845, -16.90412932818451353, 11.49999999999998934 ) ) ;
#82455=CARTESIAN_POINT ( 'NONE',  ( -94.52287095715007581, -23.72773821059536203, 11.05748984161097681 ) ) ;
#82456=CARTESIAN_POINT ( 'NONE',  ( 19.69962056004252560, 1.334664424591413434, -1.500000000000002220 ) ) ;
#82457=CARTESIAN_POINT ( 'NONE',  ( -42.57643649038576683, -24.65952944569304606, 1.056160979905694353 ) ) ;
#82458=EDGE_CURVE ( 'NONE', #69448, #57047, #84828, .T. ) ;
#82462=CARTESIAN_POINT ( 'NONE',  ( 20.01179378540625819, 5.277757631783551950, 11.49999999999999645 ) ) ;
#82463=CARTESIAN_POINT ( 'NONE',  ( -39.53777310077231277, -25.31628728160307062, 5.501674862403532984 ) ) ;
#82464=B_SPLINE_CURVE_WITH_KNOTS ( 'NONE', 3,
 ( #74404, #97738, #4898, #13492 ),
 .UNSPECIFIED., .F., .F.,
 ( 4, 4 ),
 ( 0.9204431904296468403, 0.9294496217017622630 ),
 .UNSPECIFIED. ) ;
#82467=CARTESIAN_POINT ( 'NONE',  ( 13.37577147909557773, 18.27418014603220442, 11.49999999999999645 ) ) ;
#82468=ORIENTED_EDGE ( 'NONE', *, *, #30265, .F. ) ;
#82470=CARTESIAN_POINT ( 'NONE',  ( -42.55620429048337883, -23.47596703998600276, 11.44779298504227505 ) ) ;
#82471=CARTESIAN_POINT ( 'NONE',  ( -54.62287095715005592, -23.48786465467240347, 11.44779295918255180 ) ) ;
#82472=CARTESIAN_POINT ( 'NONE',  ( -45.58953762381671737, -25.00158670708909270, 2.256160236439164635 ) ) ;
#82474=ORIENTED_EDGE ( 'NONE', *, *, #45551, .T. ) ;
#82475=EDGE_CURVE ( 'NONE', #76238, #23353, #78699, .T. ) ;
#82476=CARTESIAN_POINT ( 'NONE',  ( -99.29687923781919778, -25.25133594952260552, 6.149712203147405631 ) ) ;
#82477=CARTESIAN_POINT ( 'NONE',  ( -22.64140897529919272, -3.284158816904186651, 11.49999999999998934 ) ) ;
#82478=CARTESIAN_POINT ( 'NONE',  ( -29.49551725617323328, -24.06847746220421769, -0.2315648265717072385 ) ) ;
#82479=CARTESIAN_POINT ( 'NONE',  ( 8.794441374123232791, -19.68457759291379716, -1.500000000000002220 ) ) ;
#82480=CARTESIAN_POINT ( 'NONE',  ( -113.6312462389022215, -23.48786465467241413, 11.44779295918254292 ) ) ;
#82482=CARTESIAN_POINT ( 'NONE',  ( -22.13300264024875119, -4.194623038110560032, 11.49999999999999645 ) ) ;
#82483=ORIENTED_EDGE ( 'NONE', *, *, #669, .T. ) ;
#82485=CARTESIAN_POINT ( 'NONE',  ( 21.11370014442628218, -6.196533921283487345, 11.49999999999998934 ) ) ;
#82486=CARTESIAN_POINT ( 'NONE',  ( -44.65453377568969273, -23.73791477778911130, 11.05961554403170943 ) ) ;
#82487=CARTESIAN_POINT ( 'NONE',  ( -40.99321688279000853, -25.29087056432008040, 2.933756326319171936 ) ) ;
#82490=CARTESIAN_POINT ( 'NONE',  ( -90.58763137661625819, -24.63419186844611275, 9.035850630976923981 ) ) ;
#82494=ORIENTED_EDGE ( 'NONE', *, *, #7505, .T. ) ;
#82496=ORIENTED_EDGE ( 'NONE', *, *, #75431, .T. ) ;
#82497=CARTESIAN_POINT ( 'NONE',  ( -110.9228709571500673, -23.47596703998600631, 11.44779298504227860 ) ) ;
#82498=CARTESIAN_POINT ( 'NONE',  ( -72.52287095715007581, -23.47596703998600631, 11.44779298504228748 ) ) ;
#82500=CARTESIAN_POINT ( 'NONE',  ( -5.688044216684545518, -19.60349290560521140, -1.500000000000002220 ) ) ;
#82501=VERTEX_POINT ( 'NONE', #31265 ) ;
#82503=VECTOR ( 'NONE', #83264, 1000.000000000000114 ) ;
#82505=CARTESIAN_POINT ( 'NONE',  ( -105.6317619491183564, -24.15503026093913164, -0.2815557561904565298 ) ) ;
#82506=CARTESIAN_POINT ( 'NONE',  ( -60.52287095715006160, -29.50250243563736774, 8.947779886222145151 ) ) ;
#82507=ORIENTED_EDGE ( 'NONE', *, *, #30972, .F. ) ;
#82509=CARTESIAN_POINT ( 'NONE',  ( -28.13918514477506250, -25.26248066575644202, 8.204674103034470534 ) ) ;
#82510=B_SPLINE_CURVE_WITH_KNOTS ( 'NONE', 3,
 ( #79180, #85802, #86295, #9171 ),
 .UNSPECIFIED., .F., .F.,
 ( 4, 4 ),
 ( 0.000000000000000000, 0.003057692307692316813 ),
 .UNSPECIFIED. ) ;
#82511=EDGE_LOOP ( 'NONE', ( #46699, #79886, #78637, #47070 ) ) ;
#82513=CARTESIAN_POINT ( 'NONE',  ( 1.081820405348005165, -20.78239343107542680, -1.500000000000002220 ) ) ;
#82514=ORIENTED_EDGE ( 'NONE', *, *, #22731, .F. ) ;
#82518=CARTESIAN_POINT ( 'NONE',  ( -68.52287095715009002, -23.72773821059536914, 11.05748984161097503 ) ) ;
#82519=CARTESIAN_POINT ( 'NONE',  ( -56.62287095715008434, -23.47596703998600276, 11.44779298504227683 ) ) ;
#82520=ORIENTED_EDGE ( 'NONE', *, *, #88054, .T. ) ;
#82522=CARTESIAN_POINT ( 'NONE',  ( -78.62287095715005592, -23.96127896941632685, -0.6493128931037862595 ) ) ;
#82523=AXIS2_PLACEMENT_3D ( 'NONE', #26581, #73254, #41300 ) ;
#82524=CARTESIAN_POINT ( 'NONE',  ( -76.52287095715006160, -24.50321055353806088, 9.387540953477531147 ) ) ;
#82525=CARTESIAN_POINT ( 'NONE',  ( -86.52287095715006160, -24.64898659630367916, 1.056161002820827921 ) ) ;
#82526=CARTESIAN_POINT ( 'NONE',  ( -71.30164606794451743, -25.31201765511177726, 6.118441077956825680 ) ) ;
#82527=CARTESIAN_POINT ( 'NONE',  ( 13.47465251475156656, -17.59220275312388182, 11.49999999999999645 ) ) ;
#82529=LINE ( 'NONE', #21120, #7407 ) ;
#82530=CARTESIAN_POINT ( 'NONE',  ( 3.115699594417459473, -22.39947108414558485, 11.49999999999998934 ) ) ;
#82532=EDGE_CURVE ( 'NONE', #81122, #95482, #4870, .T. ) ;
#82533=ADVANCED_FACE ( 'NONE', ( #19540 ), #62953, .T. ) ;
#82534=CARTESIAN_POINT ( 'NONE',  ( -119.6228709571500559, -29.50248528299804818, 1.056150453629045360 ) ) ;
#82539=B_SPLINE_SURFACE_WITH_KNOTS ( 'NONE', 3, 3, ( 
 ( #24931, #8720, #33060, #17832 ),
 ( #77704, #47283, #7707, #92935 ),
 ( #23930, #38655, #56414, #64037 ),
 ( #87333, #63020, #47786, #54897 ),
 ( #9205, #31039, #8217, #70613 ),
 ( #55910, #71121, #48797, #78698 ),
 ( #78210, #40167, #39156, #85837 ) ),
 .UNSPECIFIED., .F., .F., .F.,
 ( 4, 3, 4 ),
 ( 4, 4 ),
 ( 0.7945040050992244751, 0.8970133687736503436, 0.9995227324480762121 ),
 ( 0.5096234996380107907, 0.5108715002186055010 ),
 .UNSPECIFIED. ) ;
#82540=CARTESIAN_POINT ( 'NONE',  ( -57.56702574412142326, -23.48786465467241413, 11.44779295918254647 ) ) ;
#82541=VERTEX_POINT ( 'NONE', #89065 ) ;
#82542=CARTESIAN_POINT ( 'NONE',  ( -40.49165087243459737, -25.29345418843569959, 5.543942880831776776 ) ) ;
#82543=CARTESIAN_POINT ( 'NONE',  ( 18.42719714020066846, 12.55551944762973626, -1.500000000000002220 ) ) ;
#82549=CARTESIAN_POINT ( 'NONE',  ( -27.33464509059021808, -24.58538552835475599, 1.660569724630185151 ) ) ;
#82550=FACE_OUTER_BOUND ( 'NONE', #97740, .T. ) ;
#82551=DIRECTION ( 'NONE',  ( -3.773278334453079618E-23, 0.9999999999976377785, 2.173523156925978705E-06 ) ) ;
#82552=EDGE_CURVE ( 'NONE', #32470, #79556, #73880, .T. ) ;
#82553=CARTESIAN_POINT ( 'NONE',  ( -12.10551386448753064, 15.32171617432465816, -1.500000000000002220 ) ) ;
#82554=CARTESIAN_POINT ( 'NONE',  ( -3.867184171070207288, -21.11305558764578194, -1.500000000000002220 ) ) ;
#82557=FACE_OUTER_BOUND ( 'NONE', #57709, .T. ) ;
#82558=B_SPLINE_CURVE_WITH_KNOTS ( 'NONE', 3,
 ( #91140, #66836, #66339, #59209, #21615, #74426 ),
 .UNSPECIFIED., .F., .F.,
 ( 4, 2, 4 ),
 ( 1.570755371633679342E-05, 0.001396183895866085801, 0.002776660238015834711 ),
 .UNSPECIFIED. ) ;
#82559=CARTESIAN_POINT ( 'NONE',  ( -18.67006117854901959, 13.05921059288911934, -1.500000000000002220 ) ) ;
#82560=ADVANCED_FACE ( 'NONE', ( #73834 ), #47551, .T. ) ;
#82562=CARTESIAN_POINT ( 'NONE',  ( -96.62356415693166412, -24.66019654487199375, 8.947790411086115725 ) ) ;
#82563=CARTESIAN_POINT ( 'NONE',  ( -95.52287095715006160, -29.50250243563736774, 8.947779886222138046 ) ) ;
#82564=CARTESIAN_POINT ( 'NONE',  ( 11.47056939498152950, -16.38825109899074661, 11.49999999999999645 ) ) ;
#82565=CARTESIAN_POINT ( 'NONE',  ( -50.52287095715006160, -25.00158670708909270, 2.256160236439166411 ) ) ;
#82566=VECTOR ( 'NONE', #71276, 1000.000000000000227 ) ;
#82567=CARTESIAN_POINT ( 'NONE',  ( -74.50328731481324951, -24.35071581493544102, 9.817618358456019934 ) ) ;
#82570=FACE_OUTER_BOUND ( 'NONE', #93627, .T. ) ;
#82571=CARTESIAN_POINT ( 'NONE',  ( -65.52287095715000476, -24.83620972994591369, 8.398175272781367440 ) ) ;
#82573=CARTESIAN_POINT ( 'NONE',  ( 10.00111611332133421, -19.26892646806700071, -1.500000000000002220 ) ) ;
#82574=CARTESIAN_POINT ( 'NONE',  ( -66.62287095715005592, -24.64898659630367916, 1.056161002820824368 ) ) ;
#82576=CARTESIAN_POINT ( 'NONE',  ( -17.32436372870746055, -8.985247798433253053, -1.500000000000002220 ) ) ;
#82577=LINE ( 'NONE', #14560, #45864 ) ;
#82578=EDGE_CURVE ( 'NONE', #50194, #46174, #27869, .T. ) ;
#82579=EDGE_CURVE ( 'NONE', #79632, #77615, #37571, .T. ) ;
#82581=ORIENTED_EDGE ( 'NONE', *, *, #34657, .T. ) ;
#82583=VECTOR ( 'NONE', #36936, 1000.000000000000114 ) ;
#82584=B_SPLINE_CURVE_WITH_KNOTS ( 'NONE', 3,
 ( #49718, #33974, #12122, #97374 ),
 .UNSPECIFIED., .F., .F.,
 ( 4, 4 ),
 ( 0.000000000000000000, 0.0004038461538460880185 ),
 .UNSPECIFIED. ) ;
#82585=CARTESIAN_POINT ( 'NONE',  ( -91.58383516866236107, -24.66019654487199730, 8.947790411086115725 ) ) ;
#82586=CARTESIAN_POINT ( 'NONE',  ( -104.6228709571500559, -23.48786465467241413, 11.44779295918254114 ) ) ;
#82587=CARTESIAN_POINT ( 'NONE',  ( 13.99439195134931069, 14.96789054323355828, 11.49999999999999645 ) ) ;
#82590=VECTOR ( 'NONE', #46843, 1000.000000000000114 ) ;
#82593=CARTESIAN_POINT ( 'NONE',  ( -39.44774024104455634, -25.28892609849237161, 4.157779804617712571 ) ) ;
#82595=CARTESIAN_POINT ( 'NONE',  ( -123.5228709571500190, -24.33927499327855415, 9.819080762295801179 ) ) ;
#82596=ORIENTED_EDGE ( 'NONE', *, *, #61054, .F. ) ;
#82597=CARTESIAN_POINT ( 'NONE',  ( -61.62287095715004881, -29.50250786944525672, 11.44777988621623876 ) ) ;
#82598=CARTESIAN_POINT ( 'NONE',  ( -19.45891602060003578, 12.32625358835968576, 11.49999999999999645 ) ) ;
#82599=CARTESIAN_POINT ( 'NONE',  ( 4.306090731860143350, 22.38281141545218844, -1.500000000000002220 ) ) ;
#82601=LINE ( 'NONE', #20194, #96569 ) ;
#82602=CARTESIAN_POINT ( 'NONE',  ( -59.80072539165945500, -25.13069340115295702, 2.947789388436138580 ) ) ;
#82603=CARTESIAN_POINT ( 'NONE',  ( -108.8968792378192063, -25.15277794460069316, 6.986250878905963191 ) ) ;
#82604=CARTESIAN_POINT ( 'NONE',  ( -110.5923969822278963, -24.15503026093913519, -0.2815557561904549755 ) ) ;
#82605=CARTESIAN_POINT ( 'NONE',  ( 9.607415760296678542, -19.69187540195887465, 11.49999999999998934 ) ) ;
#82608=CARTESIAN_POINT ( 'NONE',  ( -94.62287095715005592, -23.48786465467241769, 11.44779295918254114 ) ) ;
#82610=VERTEX_POINT ( 'NONE', #21030 ) ;
#82611=CARTESIAN_POINT ( 'NONE',  ( 9.418145840992488971, -18.15903486995133065, -1.500000000000002220 ) ) ;
#82616=CARTESIAN_POINT ( 'NONE',  ( -22.90524134523018773, 2.401388714834002069, -1.500000000000002220 ) ) ;
#82617=FACE_OUTER_BOUND ( 'NONE', #63849, .T. ) ;
#82618=CARTESIAN_POINT ( 'NONE',  ( -2.479824388263708990, 20.08073137130260122, -1.500000000000002220 ) ) ;
#82619=EDGE_LOOP ( 'NONE', ( #41614, #39521, #95317, #80123 ) ) ;
#82620=DIRECTION ( 'NONE',  ( 0.000000000000000000, -2.173523156925980399E-06, 0.9999999999976378895 ) ) ;
#82621=CARTESIAN_POINT ( 'NONE',  ( -46.55620429048340014, -24.64898659630528854, 1.056161002820822370 ) ) ;
#82622=DIRECTION ( 'NONE',  ( -3.773278334453079618E-23, 0.9999999999976377785, 2.173523156925979975E-06 ) ) ;
#82624=CARTESIAN_POINT ( 'NONE',  ( 19.99082695160776169, -7.785253749782737209, 11.49999999999999645 ) ) ;
#82626=DIRECTION ( 'NONE',  ( 0.000000000000000000, -0.9999999999976377785, -2.173523156925979975E-06 ) ) ;
#82627=ORIENTED_EDGE ( 'NONE', *, *, #28732, .T. ) ;
#82628=CARTESIAN_POINT ( 'NONE',  ( 18.07686251855496096, -12.98574554580779861, -1.500000000000002220 ) ) ;
#82629=CARTESIAN_POINT ( 'NONE',  ( 15.29587703590233971, -13.95322596517325664, -1.500000000000002220 ) ) ;
#82632=CARTESIAN_POINT ( 'NONE',  ( -28.61148055913008292, -23.58117181907939752, -1.055554491438110309 ) ) ;
#82634=EDGE_CURVE ( 'NONE', #71054, #99388, #92019, .T. ) ;
#82637=EDGE_CURVE ( 'NONE', #3013, #4528, #22018, .T. ) ;
#82638=CARTESIAN_POINT ( 'NONE',  ( -20.37482282770194075, 4.769447832466558346, -1.500000000000002220 ) ) ;
#82639=CARTESIAN_POINT ( 'NONE',  ( 1.740910633133015972, 21.82039641801506846, 11.49999999999999645 ) ) ;
#82641=FACE_OUTER_BOUND ( 'NONE', #74241, .T. ) ;
#82642=CARTESIAN_POINT ( 'NONE',  ( -20.59131556071872282, -9.131246169528550283, 11.49999999999998934 ) ) ;
#82643=AXIS2_PLACEMENT_3D ( 'NONE', #6774, #31108, #47348 ) ;
#82645=CARTESIAN_POINT ( 'NONE',  ( 11.42219733811748306, 17.55150860717643724, 11.49999999999998934 ) ) ;
#82647=EDGE_CURVE ( 'NONE', #28343, #79556, #43887, .T. ) ;
#82648=CARTESIAN_POINT ( 'NONE',  ( -119.5547922413071689, -24.15620529776629510, 10.23563542870659582 ) ) ;
#82649=DIRECTION ( 'NONE',  ( 0.000000000000000000, 0.9999999999976377785, 2.173523156925979975E-06 ) ) ;
#82650=EDGE_LOOP ( 'NONE', ( #98, #1735, #39226, #51975 ) ) ;
#82651=VECTOR ( 'NONE', #19726, 1000.000000000000114 ) ;
#82654=EDGE_LOOP ( 'NONE', ( #46283, #78237, #4933, #21388 ) ) ;
#82655=CARTESIAN_POINT ( 'NONE',  ( -66.55943415735386282, -23.73766607897669800, -1.055555164236460897 ) ) ;
#82657=CARTESIAN_POINT ( 'NONE',  ( 20.36625868517733196, 6.724766957447481097, -1.500000000000002220 ) ) ;
#82658=DIRECTION ( 'NONE',  ( -0.000000000000000000, 2.173523156925979552E-06, -0.9999999999976378895 ) ) ;
#82659=ORIENTED_EDGE ( 'NONE', *, *, #28466, .F. ) ;
#82660=CARTESIAN_POINT ( 'NONE',  ( -15.55823947972799282, -14.28038451723262270, 11.49999999999998934 ) ) ;
#82662=CARTESIAN_POINT ( 'NONE',  ( -118.6228709571500701, -24.65952944569305316, 1.056160979905706565 ) ) ;
#82663=CARTESIAN_POINT ( 'NONE',  ( -100.5228709571500332, -24.63287334234179227, 0.9662140553045398539 ) ) ;
#82666=CARTESIAN_POINT ( 'NONE',  ( -15.83042281971428977, -15.45127431894796466, -1.500000000000002220 ) ) ;
#82670=CARTESIAN_POINT ( 'NONE',  ( -34.52287095715006160, -23.47593901973090169, -1.443836447538997314 ) ) ;
#82672=CARTESIAN_POINT ( 'NONE',  ( -110.9909297185884327, -29.50249817218807635, 6.986241424688308221 ) ) ;
#82674=CARTESIAN_POINT ( 'NONE',  ( -5.977879402576776968, -18.46583800616800630, 11.49999999999998934 ) ) ;
#82675=CARTESIAN_POINT ( 'NONE',  ( 8.224165413489119558, 19.69228431130148493, 11.49999999999998934 ) ) ;
#82677=CARTESIAN_POINT ( 'NONE',  ( -52.62287095715005592, -23.48783264082478794, -1.443836473390070596 ) ) ;
#82678=CARTESIAN_POINT ( 'NONE',  ( -113.5228709571500616, -29.50248528299804818, 1.056150453629043584 ) ) ;
#82679=FACE_OUTER_BOUND ( 'NONE', #18002, .T. ) ;
#82680=CARTESIAN_POINT ( 'NONE',  ( -2.075279548881721947, -22.52154899835045043, -1.500000000000002220 ) ) ;
#82681=ORIENTED_EDGE ( 'NONE', *, *, #52411, .F. ) ;
#82683=CARTESIAN_POINT ( 'NONE',  ( -79.59201494684876366, -24.15543982623907127, -0.2315651400026654261 ) ) ;
#82684=CARTESIAN_POINT ( 'NONE',  ( 4.927431051831622000, -19.18327824014073357, 11.49999999999999645 ) ) ;
#82686=DIRECTION ( 'NONE',  ( -3.773278334453079030E-23, 0.9999999999976377785, 2.173523156925979128E-06 ) ) ;
#82688=CARTESIAN_POINT ( 'NONE',  ( -68.52287095715006160, -24.66019654487199730, 8.947790411086124607 ) ) ;
#82689=CARTESIAN_POINT ( 'NONE',  ( -29.22648335530837471, -25.26026456907465345, 2.413925847313246109 ) ) ;
#82691=CARTESIAN_POINT ( 'NONE',  ( 15.46703529437019853, -15.08741104398349187, -1.500000000000002220 ) ) ;
#82692=CARTESIAN_POINT ( 'NONE',  ( -26.33488822642538452, -24.88201932036028552, 6.524121876823151034 ) ) ;
#82693=CARTESIAN_POINT ( 'NONE',  ( 15.46825748771582631, 11.69065726450791409, -1.500000000000002220 ) ) ;
#82695=B_SPLINE_CURVE_WITH_KNOTS ( 'NONE', 3,
 ( #58637, #57158, #65282, #50521, #88096, #74353 ),
 .UNSPECIFIED., .F., .F.,
 ( 4, 2, 4 ),
 ( 6.384118678617110714E-06, 0.001386860460828380623, 0.002767336802978144061 ),
 .UNSPECIFIED. ) ;
#82696=CARTESIAN_POINT ( 'NONE',  ( -129.5228709571501042, -23.95044443724992789, 10.65354141964649237 ) ) ;
#82697=ADVANCED_FACE ( 'NONE', ( #8194 ), #36772, .F. ) ;
#82698=CARTESIAN_POINT ( 'NONE',  ( 12.93213199337649044, -14.99640713134888692, 11.49999999999998934 ) ) ;
#82701=CARTESIAN_POINT ( 'NONE',  ( -19.34540493331696354, 6.066486871809979142, 11.49999999999999645 ) ) ;
#82703=VECTOR ( 'NONE', #42961, 1000.000000000000114 ) ;
#82705=CARTESIAN_POINT ( 'NONE',  ( -46.58953762381672448, -24.66019654487199020, 8.947790411086131712 ) ) ;
#82707=CARTESIAN_POINT ( 'NONE',  ( -102.5474479301096693, -24.66019654487200086, 8.947790411086115725 ) ) ;
#82709=CARTESIAN_POINT ( 'NONE',  ( -44.62287095715004170, -23.73907113216990439, -1.053371485793233697 ) ) ;
#82711=LINE ( 'NONE', #12696, #94876 ) ;
#82712=CARTESIAN_POINT ( 'NONE',  ( -5.826506878040391690, 19.21762618028343184, 11.49999999999998934 ) ) ;
#82713=CARTESIAN_POINT ( 'NONE',  ( -79.58953762381673869, -23.47593901973091235, -1.443836447539004642 ) ) ;
#82714=VERTEX_POINT ( 'NONE', #90058 ) ;
#82716=CARTESIAN_POINT ( 'NONE',  ( 0.7049041324096299022, -22.85584899170066109, 11.49999999999999645 ) ) ;
#82717=CARTESIAN_POINT ( 'NONE',  ( -106.2228709571500644, -23.47593901973090524, -1.443836447538996648 ) ) ;
#82720=AXIS2_PLACEMENT_3D ( 'NONE', #56672, #96221, #26705 ) ;
#82723=CARTESIAN_POINT ( 'NONE',  ( -90.52287095715009002, -23.48783264082477373, -1.443836473390088582 ) ) ;
#82724=CARTESIAN_POINT ( 'NONE',  ( -22.40390758644239710, -1.035154934579901820, 11.49999999999999645 ) ) ;
#82725=CARTESIAN_POINT ( 'NONE',  ( -87.52287095715006160, -29.50250786944525672, 11.44777988621623344 ) ) ;
#82726=VERTEX_POINT ( 'NONE', #36278 ) ;
#82727=CARTESIAN_POINT ( 'NONE',  ( 2.178911383790714584, -20.24183328246387958, 11.49999999999998934 ) ) ;
#82728=ORIENTED_EDGE ( 'NONE', *, *, #67363, .F. ) ;
#82729=CARTESIAN_POINT ( 'NONE',  ( -3.094460115123966570, -22.75893099265358188, -1.500000000000002220 ) ) ;
#82730=B_SPLINE_CURVE_WITH_KNOTS ( 'NONE', 3,
 ( #63497, #48765, #72597, #79691, #94418, #42159 ),
 .UNSPECIFIED., .F., .F.,
 ( 4, 2, 4 ),
 ( 3.258661033901071854E-05, 0.002748063894075334409, 0.005463541177811657469 ),
 .UNSPECIFIED. ) ;
#82731=DIRECTION ( 'NONE',  ( 0.000000000000000000, 0.9999999999976377785, 2.173523156925979128E-06 ) ) ;
#82732=ORIENTED_EDGE ( 'NONE', *, *, #41328, .F. ) ;
#82733=CARTESIAN_POINT ( 'NONE',  ( -108.5228709571500616, -23.73934037231757443, 11.05740245334328087 ) ) ;
#82734=CARTESIAN_POINT ( 'NONE',  ( -94.62287095715005592, -23.48783264082478794, -1.443836473390063491 ) ) ;
#82735=LINE ( 'NONE', #13217, #52906 ) ;
#82736=CARTESIAN_POINT ( 'NONE',  ( -4.916304867406160461, -20.68799595667769964, 11.49999999999999645 ) ) ;
#82739=CARTESIAN_POINT ( 'NONE',  ( -10.57539506955483333, 19.50334513348995813, -1.500000000000002220 ) ) ;
#82740=CARTESIAN_POINT ( 'NONE',  ( -18.12278953325389708, -9.833843834435361586, 11.49999999999998934 ) ) ;
#82741=EDGE_LOOP ( 'NONE', ( #29784, #17256, #5009, #96845 ) ) ;
#82742=ORIENTED_EDGE ( 'NONE', *, *, #42788, .F. ) ;
#82745=ORIENTED_EDGE ( 'NONE', *, *, #16778, .T. ) ;
#82748=ORIENTED_EDGE ( 'NONE', *, *, #69276, .T. ) ;
#82749=CARTESIAN_POINT ( 'NONE',  ( -124.6623382465025145, -25.28334050553294432, 4.245309122437063820 ) ) ;
#82750=CARTESIAN_POINT ( 'NONE',  ( -28.62375899609942564, -24.50739853925337641, 8.947790409070465856 ) ) ;
#82752=CARTESIAN_POINT ( 'NONE',  ( 20.29938135082171158, -4.300543036493735372, -1.500000000000002220 ) ) ;
#82753=CARTESIAN_POINT ( 'NONE',  ( -8.443908442993951269, 20.02826104456839218, 11.49999999999999645 ) ) ;
#82754=ORIENTED_EDGE ( 'NONE', *, *, #84148, .F. ) ;
#82756=CARTESIAN_POINT ( 'NONE',  ( -100.4849985857635630, -25.18518816741224953, 3.295769164467318824 ) ) ;
#82757=CARTESIAN_POINT ( 'NONE',  ( -34.52287095715006160, -23.47596703998600631, 11.44779298504229459 ) ) ;
#82758=CARTESIAN_POINT ( 'NONE',  ( -115.6263010057922429, -24.52300882791528736, 0.6510814631126266017 ) ) ;
#82759=CARTESIAN_POINT ( 'NONE',  ( -22.40390758644239710, -1.035154934579901820, 11.49999999999998934 ) ) ;
#82761=CARTESIAN_POINT ( 'NONE',  ( -51.08807254026520184, -25.26334689473844364, 4.449946248032227381 ) ) ;
#82763=LINE ( 'NONE', #74163, #90620 ) ;
#82766=VERTEX_POINT ( 'NONE', #56892 ) ;
#82772=CARTESIAN_POINT ( 'NONE',  ( 7.794017451908327843, -19.83292067980804774, -1.500000000000002220 ) ) ;
#82773=ORIENTED_EDGE ( 'NONE', *, *, #98023, .F. ) ;
#82775=CARTESIAN_POINT ( 'NONE',  ( 13.92123049006271707, -16.85212209846622855, 11.49999999999998934 ) ) ;
#82777=CARTESIAN_POINT ( 'NONE',  ( 21.16149768242404861, -8.233860041645145955, -1.500000000000002220 ) ) ;
#82778=CARTESIAN_POINT ( 'NONE',  ( -41.24137195392557942, -25.28892493134095432, 3.620793846790061554 ) ) ;
#82780=CARTESIAN_POINT ( 'NONE',  ( -3.149188516569510377, 21.71089317892358395, -1.500000000000002220 ) ) ;
#82781=LINE ( 'NONE', #13263, #81954 ) ;
#82783=CARTESIAN_POINT ( 'NONE',  ( -40.33347935548481189, -25.29368123691946479, 5.540415114266751040 ) ) ;
#82785=VERTEX_POINT ( 'NONE', #10701 ) ;
#82786=PLANE ( 'NONE',  #14072 ) ;
#82790=CARTESIAN_POINT ( 'NONE',  ( -10.26558916711599778, -22.69538807860070406, 0.04347934593173622547 ) ) ;
#82791=CARTESIAN_POINT ( 'NONE',  ( -20.53569570583907122, -5.550916044964551155, -1.500000000000002220 ) ) ;
#82792=CARTESIAN_POINT ( 'NONE',  ( -112.5934586508881523, -23.73766607897671577, -1.055555164236427590 ) ) ;
#82794=CARTESIAN_POINT ( 'NONE',  ( -85.51575671001552337, -23.85016227208579664, -0.8807180028928368598 ) ) ;
#82795=CARTESIAN_POINT ( 'NONE',  ( -93.52287095715006160, -29.50247984919015209, -1.443849546365051806 ) ) ;
#82797=ORIENTED_EDGE ( 'NONE', *, *, #43509, .T. ) ;
#82798=CARTESIAN_POINT ( 'NONE',  ( -5.392953615240748455, 18.82278424538476713, 11.49999999999999645 ) ) ;
#82799=CARTESIAN_POINT ( 'NONE',  ( -40.52287095715006870, -29.50250786944525672, 11.44777988621624232 ) ) ;
#82800=CARTESIAN_POINT ( 'NONE',  ( -91.15361000704997707, -25.26877915520014639, 5.947789088310639904 ) ) ;
#82803=CARTESIAN_POINT ( 'NONE',  ( -100.8159136911362594, -25.03998861187190172, 7.529830385290721573 ) ) ;
#82804=CARTESIAN_POINT ( 'NONE',  ( -27.70544111104076990, -24.65058036537550024, 8.251826706788236265 ) ) ;
#82805=CARTESIAN_POINT ( 'NONE',  ( -50.13103505045899766, -25.12667166846206257, 7.080526547379527358 ) ) ;
#82806=CARTESIAN_POINT ( 'NONE',  ( -17.00503767097633556, -9.977476526402845991, 11.49999999999998934 ) ) ;
#82807=B_SPLINE_CURVE_WITH_KNOTS ( 'NONE', 3,
 ( #90634, #67310, #20617, #82519 ),
 .UNSPECIFIED., .F., .F.,
 ( 4, 4 ),
 ( 0.2589468163131236067, 0.2599475633538891883 ),
 .UNSPECIFIED. ) ;
#82810=CARTESIAN_POINT ( 'NONE',  ( -104.5228709571500758, -23.47596703998600631, 11.44779298504228215 ) ) ;
#82812=ADVANCED_FACE ( 'NONE', ( #41663 ), #87825, .F. ) ;
#82813=ORIENTED_EDGE ( 'NONE', *, *, #32939, .F. ) ;
#82814=CARTESIAN_POINT ( 'NONE',  ( -54.52287095715009713, -24.33927499327855770, 9.819080762295813614 ) ) ;
#82816=CARTESIAN_POINT ( 'NONE',  ( -55.51141851980899844, -23.85016227208578954, -0.8807180028928371929 ) ) ;
#82817=FACE_OUTER_BOUND ( 'NONE', #33582, .T. ) ;
#82818=CARTESIAN_POINT ( 'NONE',  ( -45.52287095715006160, -24.99156044556202616, 7.747789690856173195 ) ) ;
#82819=FACE_OUTER_BOUND ( 'NONE', #56092, .T. ) ;
#82820=B_SPLINE_CURVE_WITH_KNOTS ( 'NONE', 3,
 ( #43776, #90439, #51385, #51890 ),
 .UNSPECIFIED., .F., .F.,
 ( 4, 4 ),
 ( 0.3200144389552843638, 0.3290208702273997865 ),
 .UNSPECIFIED. ) ;
#82821=CARTESIAN_POINT ( 'NONE',  ( -120.5228709571500616, -23.47593901973090524, -1.443836447538996204 ) ) ;
#82822=CARTESIAN_POINT ( 'NONE',  ( -14.92271332039470444, 13.28099397388983327, 11.49999999999998934 ) ) ;
#82823=EDGE_CURVE ( 'NONE', #20070, #17632, #19419, .T. ) ;
#82825=CARTESIAN_POINT ( 'NONE',  ( -0.06124857980327405582, -22.25708900282751301, 9.349680052484377057 ) ) ;
#82826=ORIENTED_EDGE ( 'NONE', *, *, #5788, .T. ) ;
#82829=CARTESIAN_POINT ( 'NONE',  ( -119.6284910101131942, -23.48783264082477018, -1.443836473390087916 ) ) ;
#82830=LINE ( 'NONE', #83332, #2170 ) ;
#82832=CARTESIAN_POINT ( 'NONE',  ( -81.55862812813013818, -23.73766607897671221, -1.055555164236432919 ) ) ;
#82833=AXIS2_PLACEMENT_3D ( 'NONE', #85932, #70208, #7295 ) ;
#82834=CARTESIAN_POINT ( 'NONE',  ( -119.6228709571500559, -23.47593901973091235, -1.443836447538997536 ) ) ;
#82838=CARTESIAN_POINT ( 'NONE',  ( -68.52287095715006160, -29.50247984919015209, -1.443849546365055359 ) ) ;
#82839=CARTESIAN_POINT ( 'NONE',  ( -127.5556656467780812, -24.15543982623907837, -0.2315651400026539075 ) ) ;
#82840=ORIENTED_EDGE ( 'NONE', *, *, #70640, .T. ) ;
#82841=CARTESIAN_POINT ( 'NONE',  ( -18.13051092187696156, -9.059970205480309957, 11.49999999999998934 ) ) ;
#82843=CARTESIAN_POINT ( 'NONE',  ( -49.62287095715004881, -23.73907113216990794, -1.053371485793234807 ) ) ;
#82845=ORIENTED_EDGE ( 'NONE', *, *, #48002, .T. ) ;
#82846=PLANE ( 'NONE',  #90612 ) ;
#82849=CARTESIAN_POINT ( 'NONE',  ( 6.297820759360134524, 19.07352124001985771, -1.500000000000002220 ) ) ;
#82850=CARTESIAN_POINT ( 'NONE',  ( -17.04133944854041616, 12.32129857345222845, 11.49999999999999645 ) ) ;
#82852=CARTESIAN_POINT ( 'NONE',  ( -28.87563289579386350, -25.03413959481116535, 6.908192424899269213 ) ) ;
#82853=CARTESIAN_POINT ( 'NONE',  ( -111.6228709571500275, -24.33927499327855415, 9.819080762295820719 ) ) ;
#82854=CARTESIAN_POINT ( 'NONE',  ( -21.42919730060085115, -5.301375089729956969, -1.500000000000002220 ) ) ;
#82855=CARTESIAN_POINT ( 'NONE',  ( 20.32696876622996029, 2.630761579057304900, -1.500000000000002220 ) ) ;
#82856=CARTESIAN_POINT ( 'NONE',  ( -39.44787993411948435, -25.31589142152604666, 4.218554769620590505 ) ) ;
#82857=CARTESIAN_POINT ( 'NONE',  ( -59.62287095715004881, -24.64898659630367916, 1.056161002820822592 ) ) ;
#82858=PLANE ( 'NONE',  #89796 ) ;
#82861=FACE_OUTER_BOUND ( 'NONE', #79898, .T. ) ;
#82866=CARTESIAN_POINT ( 'NONE',  ( -76.50398578030031160, -24.34968618360934300, 0.1864209137778858327 ) ) ;
#82867=CARTESIAN_POINT ( 'NONE',  ( -15.40095275084150117, -13.70674696055758801, -1.500000000000002220 ) ) ;
#82868=CARTESIAN_POINT ( 'NONE',  ( -21.57561264457377348, 0.06291308125064201673, 11.49999999999999645 ) ) ;
#82869=ORIENTED_EDGE ( 'NONE', *, *, #36020, .T. ) ;
#82870=CARTESIAN_POINT ( 'NONE',  ( -71.62287095715005592, -29.50250243563736774, 8.947779886222143375 ) ) ;
#82872=CARTESIAN_POINT ( 'NONE',  ( -5.491053050139323766, 21.65304554001118120, 11.49999999999998934 ) ) ;
#82873=B_SPLINE_CURVE_WITH_KNOTS ( 'NONE', 3,
 ( #95608, #66186, #89000, #4265 ),
 .UNSPECIFIED., .F., .F.,
 ( 4, 4 ),
 ( 0.000000000000000000, 9.999999999997510880E-05 ),
 .UNSPECIFIED. ) ;
#82874=CARTESIAN_POINT ( 'NONE',  ( -79.60383831484530504, -25.12205723040236904, 6.693229097001963446 ) ) ;
#82875=CARTESIAN_POINT ( 'NONE',  ( -61.62287095715004881, -24.64898659630528854, 1.056161002820822592 ) ) ;
#82876=VERTEX_POINT ( 'NONE', #48267 ) ;
#82878=CARTESIAN_POINT ( 'NONE',  ( -96.55620429048339304, -23.48786465467241058, 11.44779295918254114 ) ) ;
#82880=CARTESIAN_POINT ( 'NONE',  ( -19.94048968823238255, 6.179419890754223488, 11.49999999999998934 ) ) ;
#82881=EDGE_CURVE ( 'NONE', #41589, #34094, #75127, .T. ) ;
#82883=CARTESIAN_POINT ( 'NONE',  ( -86.54507443799202804, -24.51314013834314665, 0.6176544820404149538 ) ) ;
#82884=VERTEX_POINT ( 'NONE', #57398 ) ;
#82885=ORIENTED_EDGE ( 'NONE', *, *, #2256, .T. ) ;
#82887=CARTESIAN_POINT ( 'NONE',  ( -100.6015246471107218, -23.48786465467241413, 11.44779295918254469 ) ) ;
#82888=CARTESIAN_POINT ( 'NONE',  ( 20.91448408463407205, 2.778442817847782020, -1.500000000000002220 ) ) ;
#82890=CARTESIAN_POINT ( 'NONE',  ( -122.9228709571500531, -23.47596703998600631, 11.44779298504227860 ) ) ;
#82892=CARTESIAN_POINT ( 'NONE',  ( -48.62287095715005592, -23.73934037231756733, 11.05740245334328975 ) ) ;
#82893=CARTESIAN_POINT ( 'NONE',  ( -71.62287095715005592, -29.50248528299804818, 1.056150453629036701 ) ) ;
#82895=CARTESIAN_POINT ( 'NONE',  ( -7.892909027492730267, -20.28523913882780505, -1.500000000000002220 ) ) ;
#82896=CARTESIAN_POINT ( 'NONE',  ( -71.70379718938951896, -25.24674313106178403, 6.052014784346466669 ) ) ;
#82897=CARTESIAN_POINT ( 'NONE',  ( 21.78807519107708401, 4.755904613692067073, 11.49999999999999645 ) ) ;
#82898=VERTEX_POINT ( 'NONE', #32026 ) ;
#82900=DIRECTION ( 'NONE',  ( -3.773278334453079618E-23, 0.9999999999976377785, 2.173523156925979975E-06 ) ) ;
#82903=ORIENTED_EDGE ( 'NONE', *, *, #24573, .T. ) ;
#82905=VERTEX_POINT ( 'NONE', #79701 ) ;
#82906=CARTESIAN_POINT ( 'NONE',  ( -75.52287095715006160, -24.92579138211020151, 1.929029949965663793 ) ) ;
#82907=VECTOR ( 'NONE', #21535, 1000.000000000000114 ) ;
#82910=CARTESIAN_POINT ( 'NONE',  ( -49.12170187741904925, -25.28917234601119901, 4.199658634648916866 ) ) ;
#82911=CARTESIAN_POINT ( 'NONE',  ( -7.246369895950522277, -17.95243785538732340, 11.49999999999998934 ) ) ;
#82912=B_SPLINE_CURVE_WITH_KNOTS ( 'NONE', 3,
 ( #17811, #26427, #10196, #48773 ),
 .UNSPECIFIED., .F., .F.,
 ( 4, 4 ),
 ( 7.357964204579942986E-06, 0.001221264703421874901 ),
 .UNSPECIFIED. ) ;
#82914=ORIENTED_EDGE ( 'NONE', *, *, #78779, .F. ) ;
#82915=CARTESIAN_POINT ( 'NONE',  ( 7.305494252837257285, 17.95555029072639286, 11.49999999999999645 ) ) ;
#82920=PLANE ( 'NONE',  #72513 ) ;
#82921=CARTESIAN_POINT ( 'NONE',  ( -87.62287095715004170, -23.47596703998600631, 11.44779298504227860 ) ) ;
#82922=EDGE_CURVE ( 'NONE', #62936, #64433, #25419, .T. ) ;
#82924=CARTESIAN_POINT ( 'NONE',  ( 9.307004028210867475, 17.29072351678862418, -1.500000000000002220 ) ) ;
#82925=CARTESIAN_POINT ( 'NONE',  ( -116.5562042904833930, -24.65952944569305316, 1.056160979905706121 ) ) ;
#82927=VERTEX_POINT ( 'NONE', #17302 ) ;
#82928=CARTESIAN_POINT ( 'NONE',  ( 20.98156868870745484, 4.911575462371418510, -1.500000000000002220 ) ) ;
#82929=CARTESIAN_POINT ( 'NONE',  ( -33.50410096519379977, -23.96169478059712432, 10.65365249895719124 ) ) ;
#82930=CARTESIAN_POINT ( 'NONE',  ( -116.2228709571501213, -23.47593901973090880, -1.443836447538996870 ) ) ;
#82931=CARTESIAN_POINT ( 'NONE',  ( -50.52287095715009002, -24.82558206586149652, 1.605769216559628454 ) ) ;
#82933=CARTESIAN_POINT ( 'NONE',  ( -21.12268324108725892, 9.058254180033936009, -1.500000000000002220 ) ) ;
#82937=CARTESIAN_POINT ( 'NONE',  ( -49.49642667126946094, -25.30285855287542773, 4.744951912546983230 ) ) ;
#82938=CARTESIAN_POINT ( 'NONE',  ( 18.82035724208558491, -7.196742317222773799, 11.49999999999999645 ) ) ;
#82939=CARTESIAN_POINT ( 'NONE',  ( -108.9545715455115129, -25.28814359653987154, 4.170144815448148634 ) ) ;
#82940=CARTESIAN_POINT ( 'NONE',  ( -37.62287095715005592, -29.50250243563736774, 8.947779886222148704 ) ) ;
#82941=CARTESIAN_POINT ( 'NONE',  ( -104.5228709571500758, -24.65952944569305316, 1.056160979905702346 ) ) ;
#82942=PLANE ( 'NONE',  #19678 ) ;
#82943=CARTESIAN_POINT ( 'NONE',  ( -110.3698707892751401, -25.29779155563274173, 3.294862198595579716 ) ) ;
#82944=CARTESIAN_POINT ( 'NONE',  ( 7.713363164125232707, -18.29545692620113684, 11.49999999999998934 ) ) ;
#82945=CARTESIAN_POINT ( 'NONE',  ( -113.6268379778973951, -24.15543982623907837, -0.2315651400026574602 ) ) ;
#82946=CARTESIAN_POINT ( 'NONE',  ( 10.99584971316270732, 16.45119811332560289, -1.500000000000002220 ) ) ;
#82949=CARTESIAN_POINT ( 'NONE',  ( -67.62287095715005592, -29.50247984919015209, -1.443849546365055359 ) ) ;
#82950=CARTESIAN_POINT ( 'NONE',  ( -13.01863806243235899, 16.06808769575019014, 11.49999999999999645 ) ) ;
#82952=ADVANCED_FACE ( 'NONE', ( #71605 ), #2102, .T. ) ;
#82953=CARTESIAN_POINT ( 'NONE',  ( -97.55620429048337883, -24.64965694238574656, 8.947790433994192938 ) ) ;
#82955=PLANE ( 'NONE',  #45756 ) ;
#82956=CARTESIAN_POINT ( 'NONE',  ( 6.262736145392394427, -21.83385498489561272, 11.49999999999999645 ) ) ;
#82959=B_SPLINE_SURFACE_WITH_KNOTS ( 'NONE', 3, 3, ( 
 ( #70197, #8800, #45866, #53985 ),
 ( #93517, #22002, #46862, #47364 ),
 ( #8294, #78293, #6789, #68706 ),
 ( #7792, #93019, #84912, #23496 ),
 ( #54475, #38735, #183, #38237 ),
 ( #52985, #84419, #39239, #24012 ),
 ( #39739, #70696, #45379, #1192 ) ),
 .UNSPECIFIED., .F., .F., .F.,
 ( 4, 3, 4 ),
 ( 4, 4 ),
 ( 0.3389043335492655795, 0.5146336264641651059, 0.6903629193790645768 ),
 ( 0.8868704786767156456, 0.9154791878198447197 ),
 .UNSPECIFIED. ) ;
#82963=CARTESIAN_POINT ( 'NONE',  ( -95.62287095715005592, -23.47593901973091235, -1.443836447539001089 ) ) ;
#82964=EDGE_CURVE ( 'NONE', #94513, #2264, #69020, .T. ) ;
#82965=ORIENTED_EDGE ( 'NONE', *, *, #21798, .T. ) ;
#82966=ORIENTED_EDGE ( 'NONE', *, *, #86314, .F. ) ;
#82968=CARTESIAN_POINT ( 'NONE',  ( -15.36296916364455711, -16.94538937337987150, -1.500000000000002220 ) ) ;
#82969=CARTESIAN_POINT ( 'NONE',  ( -29.66016279085162566, -23.66217729016224780, -1.055554856561816246 ) ) ;
#82970=CARTESIAN_POINT ( 'NONE',  ( -15.49073194614445015, 15.02706685249526686, -1.500000000000002220 ) ) ;
#82971=CARTESIAN_POINT ( 'NONE',  ( -123.5886726267617917, -24.65952944569305316, 1.056160979905707897 ) ) ;
#82972=CARTESIAN_POINT ( 'NONE',  ( -50.62287095715005592, -29.50248789122583659, 2.256150453626215580 ) ) ;
#82973=AXIS2_PLACEMENT_3D ( 'NONE', #98401, #37518, #30398 ) ;
#82974=CARTESIAN_POINT ( 'NONE',  ( -18.95691745938505335, -12.16397891629814865, 11.49999999999999645 ) ) ;
#82975=EDGE_LOOP ( 'NONE', ( #91596, #92511, #42832, #67887 ) ) ;
#82976=CARTESIAN_POINT ( 'NONE',  ( -87.52287095715006160, -23.47593901973090524, -1.443836447538996648 ) ) ;
#82978=CARTESIAN_POINT ( 'NONE',  ( -13.73438224071023761, 17.16576579689093762, 11.49999999999998934 ) ) ;
#82979=CARTESIAN_POINT ( 'NONE',  ( -105.5906753045558588, -24.40133493613049964, 9.663955038902797057 ) ) ;
#82980=CARTESIAN_POINT ( 'NONE',  ( -40.81364289383298427, -25.10925777354066923, 2.874306191861136117 ) ) ;
#82981=ORIENTED_EDGE ( 'NONE', *, *, #10316, .F. ) ;
#82983=CARTESIAN_POINT ( 'NONE',  ( -90.49854335619302503, -25.00182538069146787, 7.747789668545043362 ) ) ;
#82985=CARTESIAN_POINT ( 'NONE',  ( -29.52287095715007581, -23.87575411459822305, -0.6494985517685606391 ) ) ;
#82987=ORIENTED_EDGE ( 'NONE', *, *, #28946, .F. ) ;
#82991=CARTESIAN_POINT ( 'NONE',  ( -57.56701934434523338, -23.48783264082477018, -1.443836473390095243 ) ) ;
#82992=CARTESIAN_POINT ( 'NONE',  ( 10.07161678670223637, 17.78519941539584792, -1.500000000000002220 ) ) ;
#82995=CARTESIAN_POINT ( 'NONE',  ( -30.62200344337179914, -24.13759587396041439, -0.5132947483565731828 ) ) ;
#82997=CARTESIAN_POINT ( 'NONE',  ( -79.62632635320383656, -25.20074414427590170, 3.409327697718777195 ) ) ;
#82998=CARTESIAN_POINT ( 'NONE',  ( -47.58953762381672448, -23.48786465467240703, 11.44779295918255180 ) ) ;
#82999=ORIENTED_EDGE ( 'NONE', *, *, #15219, .F. ) ;
#83000=CARTESIAN_POINT ( 'NONE',  ( -49.52287095715006160, -24.65952944569304606, 1.056160979905693686 ) ) ;
#83001=DIRECTION ( 'NONE',  ( 0.000000000000000000, 0.9999999999976377785, 2.173523156925979128E-06 ) ) ;
#83003=CARTESIAN_POINT ( 'NONE',  ( 0.4431998670617953717, 20.78131286043265646, 11.49999999999998934 ) ) ;
#83004=EDGE_CURVE ( 'NONE', #25851, #99951, #22987, .T. ) ;
#83005=ORIENTED_EDGE ( 'NONE', *, *, #98271, .T. ) ;
#83006=CARTESIAN_POINT ( 'NONE',  ( -40.41683116089613748, -25.30532407203700984, 5.082404393492757855 ) ) ;
#83008=B_SPLINE_CURVE_WITH_KNOTS ( 'NONE', 3,
 ( #49080, #87118, #79508, #57200, #34842, #2397 ),
 .UNSPECIFIED., .F., .F.,
 ( 4, 2, 4 ),
 ( 6.391158118952235087E-06, 0.001387004593080775738, 0.002767618028042598960 ),
 .UNSPECIFIED. ) ;
#83009=CARTESIAN_POINT ( 'NONE',  ( -91.23534077628073646, -25.23397913219354649, 6.409327625488847602 ) ) ;
#83011=ORIENTED_EDGE ( 'NONE', *, *, #15429, .F. ) ;
#83012=FACE_OUTER_BOUND ( 'NONE', #23069, .T. ) ;
#83015=CARTESIAN_POINT ( 'NONE',  ( -113.6228709571500559, -23.47593901973091235, -1.443836447538999312 ) ) ;
#83017=CARTESIAN_POINT ( 'NONE',  ( 19.88262469969689050, -9.776007750257504014, 11.49999999999999645 ) ) ;
#83018=ORIENTED_EDGE ( 'NONE', *, *, #27357, .T. ) ;
#83021=CARTESIAN_POINT ( 'NONE',  ( 22.61563695565308407, -1.323143620866313208, -1.500000000000002220 ) ) ;
#83023=CARTESIAN_POINT ( 'NONE',  ( -99.33845364856260574, -25.30505776661208728, 5.120429160701139182 ) ) ;
#83027=B_SPLINE_CURVE_WITH_KNOTS ( 'NONE', 3,
 ( #15262, #52837, #46219, #98993 ),
 .UNSPECIFIED., .F., .F.,
 ( 4, 4 ),
 ( 2.236995757993482539E-11, 0.0004668241723168402280 ),
 .UNSPECIFIED. ) ;
#83029=CARTESIAN_POINT ( 'NONE',  ( -4.233023369943174075, 19.68221892606961987, 11.49999999999998934 ) ) ;
#83031=ORIENTED_EDGE ( 'NONE', *, *, #74433, .T. ) ;
#83032=CARTESIAN_POINT ( 'NONE',  ( -89.52287095715004739, -23.96177878511309345, 10.65340807706329684 ) ) ;
#83033=CARTESIAN_POINT ( 'NONE',  ( -8.840690135214121170, 20.45858245768130956, -1.500000000000002220 ) ) ;
#83034=ORIENTED_EDGE ( 'NONE', *, *, #19298, .T. ) ;
#83036=CARTESIAN_POINT ( 'NONE',  ( -89.62287095715007013, -23.95044443724992433, 10.65354141964649948 ) ) ;
#83037=DIRECTION ( 'NONE',  ( -1.000000000000000000, -3.773278334444166432E-23, -8.201307841325785021E-29 ) ) ;
#83038=CARTESIAN_POINT ( 'NONE',  ( -84.58953762381672448, -24.65952944569305316, 1.056160979905704567 ) ) ;
#83040=CARTESIAN_POINT ( 'NONE',  ( -18.49313839071750820, -6.238557295281221826, -1.500000000000002220 ) ) ;
#83041=AXIS2_PLACEMENT_3D ( 'NONE', #91173, #91667, #69339 ) ;
#83042=CARTESIAN_POINT ( 'NONE',  ( 5.910897418159350103, -20.63055655796343757, 11.49999999999998934 ) ) ;
#83044=DIRECTION ( 'NONE',  ( 1.000000000000000000, 3.773278334444166432E-23, 8.201307841325785021E-29 ) ) ;
#83046=CARTESIAN_POINT ( 'NONE',  ( 13.81544771398824345, -18.15223324129861382, -1.500000000000002220 ) ) ;
#83050=CARTESIAN_POINT ( 'NONE',  ( 18.80405327530603543, -6.659971710459020144, 11.49999999999999645 ) ) ;
#83051=DIRECTION ( 'NONE',  ( -3.773278334453079030E-23, 0.9999999999976377785, 2.173523156925979128E-06 ) ) ;
#83052=CARTESIAN_POINT ( 'NONE',  ( -74.49654804551374809, -24.66019654487200441, 8.947790411086105067 ) ) ;
#83053=PLANE ( 'NONE',  #86103 ) ;
#83054=ORIENTED_EDGE ( 'NONE', *, *, #13583, .T. ) ;
#83056=CARTESIAN_POINT ( 'NONE',  ( -124.5228709571502037, -23.96127896941633750, -0.6493128931037959184 ) ) ;
#83057=CARTESIAN_POINT ( 'NONE',  ( 20.88924836996103451, 6.054424527964996194, -1.500000000000002220 ) ) ;
#83058=CARTESIAN_POINT ( 'NONE',  ( -37.58953762381672448, -23.47593901973091235, -1.443836447539011525 ) ) ;
#83059=CARTESIAN_POINT ( 'NONE',  ( 17.63768857353127828, -8.544740250177758512, -1.500000000000002220 ) ) ;
#83060=CARTESIAN_POINT ( 'NONE',  ( -99.33777189820985143, -25.23274841714367511, 6.421454660997744313 ) ) ;
#83061=B_SPLINE_CURVE_WITH_KNOTS ( 'NONE', 3,
 ( #17953, #56029, #93060, #63645 ),
 .UNSPECIFIED., .F., .F.,
 ( 4, 4 ),
 ( 2.775557561562891351E-17, 0.0001000000000000167286 ),
 .UNSPECIFIED. ) ;
#83065=CARTESIAN_POINT ( 'NONE',  ( -60.62287095715003460, -23.85229601348995843, 10.88205029486208986 ) ) ;
#83066=CARTESIAN_POINT ( 'NONE',  ( -123.6228709571500559, -23.47596703998600631, 11.44779298504227860 ) ) ;
#83067=CARTESIAN_POINT ( 'NONE',  ( 18.14102482237423075, -9.550406459077080967, 11.49999999999999645 ) ) ;
#83068=DIRECTION ( 'NONE',  ( -1.000000000000000000, -3.773278334444167608E-23, -8.201307833595939069E-29 ) ) ;
#83069=CARTESIAN_POINT ( 'NONE',  ( -42.52287095715005449, -24.66019654487199020, 8.947790411086133489 ) ) ;
#83070=EDGE_CURVE ( 'NONE', #94577, #53188, #20787, .T. ) ;
#83071=VECTOR ( 'NONE', #70713, 1000.000000000000114 ) ;
#83072=ORIENTED_EDGE ( 'NONE', *, *, #59050, .F. ) ;
#83073=CARTESIAN_POINT ( 'NONE',  ( -62.52287095715006160, -24.64965694238406613, 8.947790433994201820 ) ) ;
#83074=CARTESIAN_POINT ( 'NONE',  ( -40.42371425561744047, -25.28892422309021981, 3.294940063421055498 ) ) ;
#83076=DIRECTION ( 'NONE',  ( 0.000000000000000000, -0.9999999999976377785, -2.173523156925979975E-06 ) ) ;
#83078=DIRECTION ( 'NONE',  ( -3.773278334453079030E-23, 0.9999999999976377785, 2.173523156925979128E-06 ) ) ;
#83079=EDGE_LOOP ( 'NONE', ( #53061, #44970, #15727, #4995 ) ) ;
#83083=CARTESIAN_POINT ( 'NONE',  ( -2.116611060711651504, 22.89395876494169002, 11.49999999999999645 ) ) ;
#83084=CARTESIAN_POINT ( 'NONE',  ( -22.70586268970451371, -1.818501321912391999, 11.49999999999998934 ) ) ;
#83085=CARTESIAN_POINT ( 'NONE',  ( -110.5546867764639671, -24.15602025860899360, 10.28564288303533480 ) ) ;
#83086=B_SPLINE_SURFACE_WITH_KNOTS ( 'NONE', 3, 3, ( 
 ( #17386, #56970, #25500, #40726 ),
 ( #24989, #71684, #18388, #49357 ),
 ( #71182, #26509, #2181, #3183 ),
 ( #3675, #33113, #87397, #10781 ),
 ( #64091, #34123, #57970, #48854 ),
 ( #65095, #57473, #18881, #88406 ),
 ( #88909, #19380, #78765, #9265 ) ),
 .UNSPECIFIED., .F., .F., .F.,
 ( 4, 3, 4 ),
 ( 4, 4 ),
 ( 0.7945040050992251413, 0.8970133687736507877, 0.9995227324480765452 ),
 ( 0.7796921278179643755, 0.7810648099988581894 ),
 .UNSPECIFIED. ) ;
#83089=EDGE_CURVE ( 'NONE', #97718, #30829, #33989, .T. ) ;
#83090=PLANE ( 'NONE',  #78675 ) ;
#83091=CARTESIAN_POINT ( 'NONE',  ( -64.62287095715005592, -23.48783264082478084, -1.443836473390069042 ) ) ;
#83092=CARTESIAN_POINT ( 'NONE',  ( 21.76694381678408519, 2.417257996116004115, -1.500000000000002220 ) ) ;
#83094=CARTESIAN_POINT ( 'NONE',  ( -50.62287095715006302, -24.92579138211019085, 1.929029949965668456 ) ) ;
#83095=CARTESIAN_POINT ( 'NONE',  ( -41.46445985487523700, -25.29262591909929725, 4.252576102391492086 ) ) ;
#83097=CARTESIAN_POINT ( 'NONE',  ( -106.6228709571500559, -29.50248528299804818, 1.056150453629043584 ) ) ;
#83099=ORIENTED_EDGE ( 'NONE', *, *, #13018, .F. ) ;
#83100=B_SPLINE_CURVE_WITH_KNOTS ( 'NONE', 3,
 ( #92305, #13674, #38022, #91805, #30409, #100396 ),
 .UNSPECIFIED., .F., .F.,
 ( 4, 2, 4 ),
 ( 6.391158118963032216E-06, 0.001387004593080781809, 0.002767618028042600695 ),
 .UNSPECIFIED. ) ;
#83101=CARTESIAN_POINT ( 'NONE',  ( 20.25987197511681259, 2.754759976156288204, -1.500000000000002220 ) ) ;
#83107=ADVANCED_FACE ( 'NONE', ( #19793 ), #58877, .F. ) ;
#83108=CARTESIAN_POINT ( 'NONE',  ( 17.08057647167376913, 15.47633299359885761, -1.500000000000002220 ) ) ;
#83109=LINE ( 'NONE', #98332, #48707 ) ;
#83110=CARTESIAN_POINT ( 'NONE',  ( 17.32893120472914816, 10.46255702124672027, -1.500000000000002220 ) ) ;
#83114=DIRECTION ( 'NONE',  ( 0.000000000000000000, 0.9999999999976377785, 2.173523156925979975E-06 ) ) ;
#83115=LINE ( 'NONE', #90244, #41581 ) ;
#83116=CARTESIAN_POINT ( 'NONE',  ( -70.49056310608266074, -24.83618233451450052, 1.606449574219541487 ) ) ;
#83117=CARTESIAN_POINT ( 'NONE',  ( -21.42254595866439004, -0.3319015934494286557, 11.49999999999999645 ) ) ;
#83120=CARTESIAN_POINT ( 'NONE',  ( -41.54630002450753068, -24.15543982623907127, -0.2315651400026566831 ) ) ;
#83121=ORIENTED_EDGE ( 'NONE', *, *, #23937, .T. ) ;
#83122=CARTESIAN_POINT ( 'NONE',  ( 20.27745880512110688, -4.159726151199424571, 11.49999999999998934 ) ) ;
#83123=EDGE_CURVE ( 'NONE', #14722, #54721, #71559, .T. ) ;
#83124=ORIENTED_EDGE ( 'NONE', *, *, #14394, .T. ) ;
#83125=EDGE_CURVE ( 'NONE', #41225, #58220, #89706, .T. ) ;
#83126=CARTESIAN_POINT ( 'NONE',  ( -91.52287095715013265, -23.96177878511310055, 10.65340807706329507 ) ) ;
#83127=ORIENTED_EDGE ( 'NONE', *, *, #7207, .T. ) ;
#83130=CARTESIAN_POINT ( 'NONE',  ( 6.892386425805808514, -19.84609432511738447, -1.500000000000002220 ) ) ;
#83131=CARTESIAN_POINT ( 'NONE',  ( -1.351711525931510449, 21.94731587555429186, 11.49999999999999645 ) ) ;
#83132=EDGE_CURVE ( 'NONE', #90808, #70257, #29737, .T. ) ;
#83133=CARTESIAN_POINT ( 'NONE',  ( -37.62898825168296923, -24.51419770103156637, 9.386484678747175181 ) ) ;
#83134=CARTESIAN_POINT ( 'NONE',  ( -21.23328875057882570, -7.520457577684837247, 11.49999999999998934 ) ) ;
#83135=CARTESIAN_POINT ( 'NONE',  ( -18.84683179826791743, -9.195131953753229226, -1.500000000000002220 ) ) ;
#83138=CARTESIAN_POINT ( 'NONE',  ( -91.55620429048337883, -23.48783264082478084, -1.443836473390063713 ) ) ;
#83141=ORIENTED_EDGE ( 'NONE', *, *, #86906, .T. ) ;
#83142=B_SPLINE_CURVE_WITH_KNOTS ( 'NONE', 3,
 ( #12461, #4857, #28194, #22057 ),
 .UNSPECIFIED., .F., .F.,
 ( 4, 4 ),
 ( 0.000000000000000000, 1.000000000000000000 ),
 .UNSPECIFIED. ) ;
#83143=EDGE_CURVE ( 'NONE', #60457, #11737, #83100, .T. ) ;
#83147=B_SPLINE_CURVE_WITH_KNOTS ( 'NONE', 3,
 ( #55011, #85438, #7820, #15426, #39763, #94054 ),
 .UNSPECIFIED., .F., .F.,
 ( 4, 2, 4 ),
 ( 0.000000000000000000, 0.001380764517854764966, 0.002761529035709529931 ),
 .UNSPECIFIED. ) ;
#83148=CARTESIAN_POINT ( 'NONE',  ( -66.55386350891794223, -23.96119346886880308, -0.6495511937832151306 ) ) ;
#83149=CARTESIAN_POINT ( 'NONE',  ( -19.33005188562793819, 9.364626179424670127, -1.500000000000002220 ) ) ;
#83151=CARTESIAN_POINT ( 'NONE',  ( -81.48149462243459595, -25.23679622552714363, 6.293943003980942308 ) ) ;
#83152=EDGE_LOOP ( 'NONE', ( #9622, #53756, #65665, #25759 ) ) ;
#83153=CARTESIAN_POINT ( 'NONE',  ( -2.902382693073098707, -20.91247731031871382, 11.49999999999998934 ) ) ;
#83154=CARTESIAN_POINT ( 'NONE',  ( -99.58390386930925331, -25.25019242640517447, 3.741874911158628247 ) ) ;
#83155=CARTESIAN_POINT ( 'NONE',  ( -81.48149462243461016, -25.24685308744633261, 6.293942982122115559 ) ) ;
#83156=CARTESIAN_POINT ( 'NONE',  ( -100.5228709571500332, -24.83602698348161297, 1.605859176311263292 ) ) ;
#83158=CARTESIAN_POINT ( 'NONE',  ( -65.52287095715006160, -29.50249982740957577, 7.747779886224967605 ) ) ;
#83159=CARTESIAN_POINT ( 'NONE',  ( -14.81638660137672225, 16.44347145309322045, -1.500000000000002220 ) ) ;
#83161=PLANE ( 'NONE',  #6303 ) ;
#83162=CARTESIAN_POINT ( 'NONE',  ( -56.52287095715006870, -24.64965694238407323, 8.947790433994201820 ) ) ;
#83164=CARTESIAN_POINT ( 'NONE',  ( -41.86878170341644534, -25.31624462002888265, 4.256748773907617078 ) ) ;
#83165=CARTESIAN_POINT ( 'NONE',  ( -100.6291402768932386, -24.52300882791526959, 0.6510814631126226049 ) ) ;
#83166=CARTESIAN_POINT ( 'NONE',  ( 10.09180897563621926, 16.61094848277074476, 11.49999999999998934 ) ) ;
#83167=CARTESIAN_POINT ( 'NONE',  ( -15.71168838272081558, 14.50144224353281786, -1.500000000000002220 ) ) ;
#83172=CARTESIAN_POINT ( 'NONE',  ( 22.64978874513612439, 0.4204215919581203442, -1.500000000000002220 ) ) ;
#83173=B_SPLINE_SURFACE_WITH_KNOTS ( 'NONE', 3, 3, ( 
 ( #74775, #60079, #4286, #66207 ),
 ( #5272, #19998, #43846, #36230 ),
 ( #52454, #21476, #12380, #83386 ),
 ( #28119, #67193, #35236, #27626 ),
 ( #82394, #90016, #98108, #28614 ),
 ( #13873, #20985, #44844, #74290 ),
 ( #90508, #75768, #6268, #58572 ),
 ( #50966, #81903, #4781, #35736 ),
 ( #66707, #97618, #51459, #12872 ),
 ( #51958, #82887, #13372, #44350 ) ),
 .UNSPECIFIED., .F., .F., .F.,
 ( 4, 3, 3, 4 ),
 ( 4, 4 ),
 ( 0.7022005934544808259, 0.7765311282028796169, 0.8508616629512784080, 0.9995227324480758790 ),
 ( 0.2995301457407982260, 0.3007213865952733656 ),
 .UNSPECIFIED. ) ;
#83174=EDGE_LOOP ( 'NONE', ( #80882, #98581, #83921, #97000 ) ) ;
#83176=CARTESIAN_POINT ( 'NONE',  ( -102.6228709571500559, -24.64965695001469115, 8.947790433994178727 ) ) ;
#83177=CARTESIAN_POINT ( 'NONE',  ( -19.78623529325263775, -1.157695164950638844, 11.49999999999999645 ) ) ;
#83178=CARTESIAN_POINT ( 'NONE',  ( -59.62287095715005592, -24.51283580621365132, 0.6167428607019761477 ) ) ;
#83180=ORIENTED_EDGE ( 'NONE', *, *, #50736, .T. ) ;
#83181=CARTESIAN_POINT ( 'NONE',  ( -53.62287095715005592, -24.50321055353806798, 9.387540953477540029 ) ) ;
#83183=CARTESIAN_POINT ( 'NONE',  ( -75.52287095715010423, -24.92604778743017846, 8.074972756849359001 ) ) ;
#83184=CARTESIAN_POINT ( 'NONE',  ( 21.64940796807912449, -0.2623997510114038922, 11.49999999999998934 ) ) ;
#83185=CARTESIAN_POINT ( 'NONE',  ( -49.73634623139758304, -25.27517911410419416, 2.988891300836324039 ) ) ;
#83186=CARTESIAN_POINT ( 'NONE',  ( 17.17441491540288823, 9.109037055621362455, -1.500000000000002220 ) ) ;
#83189=CARTESIAN_POINT ( 'NONE',  ( 17.16143643543069075, 9.858047367376444825, 11.49999999999998934 ) ) ;
#83190=EDGE_LOOP ( 'NONE', ( #51215, #34837, #71217, #71894 ) ) ;
#83191=B_SPLINE_CURVE_WITH_KNOTS ( 'NONE', 3,
 ( #40196, #17354, #56939, #16346, #47312, #71151 ),
 .UNSPECIFIED., .F., .F.,
 ( 4, 2, 4 ),
 ( 1.570887131794952276E-05, 0.001396322306279766060, 0.002776935741241582344 ),
 .UNSPECIFIED. ) ;
#83192=VECTOR ( 'NONE', #68616, 1000.000000000000114 ) ;
#83193=CARTESIAN_POINT ( 'NONE',  ( -14.66855384320708033, -14.05595220846724835, 11.49999999999999645 ) ) ;
#83194=DIRECTION ( 'NONE',  ( -3.773278334453080206E-23, 0.9999999999976377785, 2.173523156925979975E-06 ) ) ;
#83195=CARTESIAN_POINT ( 'NONE',  ( -98.52287095715006160, -23.48786465467241769, 11.44779295918254114 ) ) ;
#83196=ADVANCED_FACE ( 'NONE', ( #84692 ), #22775, .T. ) ;
#83197=B_SPLINE_CURVE_WITH_KNOTS ( 'NONE', 3,
 ( #2755, #95090, #33187, #33696, #95589, #49939, #64674, #55542 ),
 .UNSPECIFIED., .F., .F.,
 ( 4, 2, 2, 4 ),
 ( 0.000000000000000000, 0.002001098010032797275, 0.003001647015049197648, 0.004002196020065598020 ),
 .UNSPECIFIED. ) ;
#83199=CARTESIAN_POINT ( 'NONE',  ( -30.59367615247571592, -24.87212640336024805, 1.420893871182737467 ) ) ;
#83201=CARTESIAN_POINT ( 'NONE',  ( -87.52287095715006160, -29.50248528299804818, 1.056150453629040253 ) ) ;
#83203=CARTESIAN_POINT ( 'NONE',  ( -95.62287095715009855, -24.15431212366392799, -0.2830839119429097717 ) ) ;
#83204=DIRECTION ( 'NONE',  ( -3.773278334453079030E-23, 0.9999999999976377785, 2.173523156925979128E-06 ) ) ;
#83205=CARTESIAN_POINT ( 'NONE',  ( -7.287290609967129740, 18.71191762695291771, -1.500000000000002220 ) ) ;
#83206=AXIS2_PLACEMENT_3D ( 'NONE', #12481, #57186, #11982 ) ;
#83208=CARTESIAN_POINT ( 'NONE',  ( -28.55620429048340725, -23.32632435101244894, -1.443835797391826548 ) ) ;
#83209=ORIENTED_EDGE ( 'NONE', *, *, #38909, .T. ) ;
#83210=CARTESIAN_POINT ( 'NONE',  ( -117.6228709571500559, -23.47596703998600631, 11.44779298504227683 ) ) ;
#83211=EDGE_CURVE ( 'NONE', #38181, #99597, #34594, .T. ) ;
#83214=CARTESIAN_POINT ( 'NONE',  ( 20.41593879258296695, -10.28030303932802880, 11.49999999999999645 ) ) ;
#83215=CARTESIAN_POINT ( 'NONE',  ( -30.47287095715008576, -25.25807433263999258, 3.875005595686505711 ) ) ;
#83216=DIRECTION ( 'NONE',  ( 0.000000000000000000, -2.173523156925980399E-06, 0.9999999999976378895 ) ) ;
#83219=CARTESIAN_POINT ( 'NONE',  ( -43.52287095715006160, -24.64965694238406613, 8.947790433994205372 ) ) ;
#83220=B_SPLINE_CURVE_WITH_KNOTS ( 'NONE', 3,
 ( #52945, #99091, #21463, #69153, #44337, #28601 ),
 .UNSPECIFIED., .F., .F.,
 ( 4, 2, 4 ),
 ( 0.000000000000000000, 0.001380764517854765182, 0.002761529035709530365 ),
 .UNSPECIFIED. ) ;
#83223=FACE_OUTER_BOUND ( 'NONE', #13684, .T. ) ;
#83224=ORIENTED_EDGE ( 'NONE', *, *, #61618, .T. ) ;
#83225=CARTESIAN_POINT ( 'NONE',  ( 14.56535739210195857, -14.21638276092092745, 11.49999999999998934 ) ) ;
#83226=VECTOR ( 'NONE', #31883, 1000.000000000000114 ) ;
#83228=B_SPLINE_CURVE_WITH_KNOTS ( 'NONE', 3,
 ( #3969, #65392, #41529, #2977, #18184, #72484 ),
 .UNSPECIFIED., .F., .F.,
 ( 4, 2, 4 ),
 ( 6.384118678608570081E-06, 0.001386860460828373684, 0.002767336802978138856 ),
 .UNSPECIFIED. ) ;
#83229=EDGE_CURVE ( 'NONE', #49573, #76836, #4419, .T. ) ;
#83230=CARTESIAN_POINT ( 'NONE',  ( 22.85142058292489153, -2.183311388647848350, 11.49999999999998934 ) ) ;
#83231=CARTESIAN_POINT ( 'NONE',  ( -115.6228709571500559, -23.48786465467242479, 11.44779295918253759 ) ) ;
#83233=CARTESIAN_POINT ( 'NONE',  ( -38.62287095715005592, -23.47593901973091235, -1.443836447539011525 ) ) ;
#83234=CARTESIAN_POINT ( 'NONE',  ( -67.52287095715004739, -24.33927499327855415, 9.819080762295804732 ) ) ;
#83236=CARTESIAN_POINT ( 'NONE',  ( -74.62287095715005592, -23.47593901973091235, -1.443836447539006196 ) ) ;
#83237=CARTESIAN_POINT ( 'NONE',  ( -7.948041996521916452, 19.69052605537007850, 11.49999999999999645 ) ) ;
#83238=ORIENTED_EDGE ( 'NONE', *, *, #11498, .F. ) ;
#83239=ORIENTED_EDGE ( 'NONE', *, *, #25437, .F. ) ;
#83240=CARTESIAN_POINT ( 'NONE',  ( -10.56713949322891999, -19.48831581008217384, -1.500000000000002220 ) ) ;
#83241=CARTESIAN_POINT ( 'NONE',  ( -13.12974562303265813, -15.89414520977026513, 11.49999999999998934 ) ) ;
#83242=EDGE_CURVE ( 'NONE', #31325, #23352, #14090, .T. ) ;
#83243=B_SPLINE_CURVE_WITH_KNOTS ( 'NONE', 3,
 ( #82129, #96357, #18233, #26346 ),
 .UNSPECIFIED., .F., .F.,
 ( 4, 4 ),
 ( 0.1899215428025058938, 0.1989279740746213720 ),
 .UNSPECIFIED. ) ;
#83244=ORIENTED_EDGE ( 'NONE', *, *, #29669, .T. ) ;
#83245=ORIENTED_EDGE ( 'NONE', *, *, #7979, .T. ) ;
#83246=DIRECTION ( 'NONE',  ( 3.773278334444167608E-23, -1.000000000000000000, 0.000000000000000000 ) ) ;
#83247=CARTESIAN_POINT ( 'NONE',  ( -36.55620429048339304, -24.64898659630528854, 1.056161002820822592 ) ) ;
#83249=ORIENTED_EDGE ( 'NONE', *, *, #55210, .F. ) ;
#83251=CARTESIAN_POINT ( 'NONE',  ( -41.63440463616400677, -24.35071581493542325, 9.817618358456032368 ) ) ;
#83252=DIRECTION ( 'NONE',  ( 0.000000000000000000, -2.173523156925979552E-06, 0.9999999999976378895 ) ) ;
#83253=CARTESIAN_POINT ( 'NONE',  ( 19.40724743217988291, -7.346346906864608783, -1.500000000000002220 ) ) ;
#83254=CARTESIAN_POINT ( 'NONE',  ( 9.495391690522565042, 19.61495305411445500, 11.49999999999999645 ) ) ;
#83256=FACE_OUTER_BOUND ( 'NONE', #60193, .T. ) ;
#83257=CARTESIAN_POINT ( 'NONE',  ( -113.6228709571501128, -23.96177878511308634, 10.65340807706329507 ) ) ;
#83258=CARTESIAN_POINT ( 'NONE',  ( -115.6235241281218009, -25.00158670708910691, 2.256160236439219258 ) ) ;
#83259=CARTESIAN_POINT ( 'NONE',  ( -16.61153998044026991, -15.06042057022924929, 11.49999999999998934 ) ) ;
#83261=CARTESIAN_POINT ( 'NONE',  ( -51.29687923781917647, -25.31296603634400100, 3.993462069187891039 ) ) ;
#83264=DIRECTION ( 'NONE',  ( -3.773278334453079618E-23, 0.9999999999976377785, 2.173523156925979975E-06 ) ) ;
#83265=CARTESIAN_POINT ( 'NONE',  ( -57.58953762381671027, -24.65952944569304250, 1.056160979905691910 ) ) ;
#83267=EDGE_LOOP ( 'NONE', ( #17459, #35829, #69467, #21507 ) ) ;
#83268=VERTEX_POINT ( 'NONE', #84780 ) ;
#83269=EDGE_CURVE ( 'NONE', #10237, #99590, #24385, .T. ) ;
#83270=CARTESIAN_POINT ( 'NONE',  ( -99.91009256315520304, -25.31150033986424575, 5.318604188631694818 ) ) ;
#83272=CARTESIAN_POINT ( 'NONE',  ( -20.53569570583907122, -5.550916044964551155, -1.500000000000002220 ) ) ;
#83275=CARTESIAN_POINT ( 'NONE',  ( 15.37114825158464271, 14.37155165002682544, -1.500000000000002220 ) ) ;
#83276=CARTESIAN_POINT ( 'NONE',  ( -82.52287095715006160, -24.64898659630367916, 1.056161002820826145 ) ) ;
#83277=CARTESIAN_POINT ( 'NONE',  ( -113.5228709571500758, -24.33927499327855770, 9.819080762295806508 ) ) ;
#83278=CARTESIAN_POINT ( 'NONE',  ( -65.52287095715010423, -24.14406661686763300, 10.28769366194077151 ) ) ;
#83279=CARTESIAN_POINT ( 'NONE',  ( -19.17877449816284496, 10.63638241594707345, -1.500000000000002220 ) ) ;
#83280=CARTESIAN_POINT ( 'NONE',  ( -87.58323434392801232, -24.65952944569305316, 1.056160979905705455 ) ) ;
#83281=ORIENTED_EDGE ( 'NONE', *, *, #48063, .T. ) ;
#83282=CARTESIAN_POINT ( 'NONE',  ( -80.44905418446258238, -25.30553335704075124, 4.507974687363522470 ) ) ;
#83284=CARTESIAN_POINT ( 'NONE',  ( -116.6228709571500559, -23.47593901973091235, -1.443836447538997536 ) ) ;
#83286=CARTESIAN_POINT ( 'NONE',  ( -10.19904455147402089, -23.73149922466213368, 6.147794833475636267 ) ) ;
#83287=CARTESIAN_POINT ( 'NONE',  ( 21.27783752795556538, -0.9766432368044721812, -1.500000000000002220 ) ) ;
#83289=CARTESIAN_POINT ( 'NONE',  ( -107.5199639939815484, -23.73791477778912551, 11.05961554403170055 ) ) ;
#83292=B_SPLINE_CURVE_WITH_KNOTS ( 'NONE', 3,
 ( #89090, #96692, #19566, #33292 ),
 .UNSPECIFIED., .F., .F.,
 ( 4, 4 ),
 ( 0.02877499693705111092, 0.02977574397781653295 ),
 .UNSPECIFIED. ) ;
#83293=CARTESIAN_POINT ( 'NONE',  ( -79.62287095715009855, -24.50321055353803956, 9.387540953477525818 ) ) ;
#83294=ORIENTED_EDGE ( 'NONE', *, *, #51037, .F. ) ;
#83295=CARTESIAN_POINT ( 'NONE',  ( -98.90284052011273275, -25.24560384201612706, 6.309255790471715919 ) ) ;
#83296=CARTESIAN_POINT ( 'NONE',  ( -17.52035102510334141, -8.822347199899118309, 11.49999999999999645 ) ) ;
#83297=CARTESIAN_POINT ( 'NONE',  ( -125.6228709571500843, -25.00158670708909625, 2.256160236439166855 ) ) ;
#83298=B_SPLINE_CURVE_WITH_KNOTS ( 'NONE', 3,
 ( #35978, #53215, #75525, #84143 ),
 .UNSPECIFIED., .F., .F.,
 ( 4, 4 ),
 ( 0.000000000000000000, 1.000000000000000000 ),
 .UNSPECIFIED. ) ;
#83301=CARTESIAN_POINT ( 'NONE',  ( -88.58842802440713626, -24.35071581493543746, 9.817618358456025263 ) ) ;
#83302=CARTESIAN_POINT ( 'NONE',  ( -101.8581997900095502, -25.20156876886343866, 6.591836956137893111 ) ) ;
#83303=CARTESIAN_POINT ( 'NONE',  ( -25.53098197642538736, -24.92569209777881056, 4.942811685741776984 ) ) ;
#83304=CARTESIAN_POINT ( 'NONE',  ( -45.62287095715004881, -24.14321612903114556, -0.2833117244521596301 ) ) ;
#83305=CARTESIAN_POINT ( 'NONE',  ( -13.01991350253972080, 14.82018230214031895, -1.500000000000002220 ) ) ;
#83306=ORIENTED_EDGE ( 'NONE', *, *, #57130, .T. ) ;
#83311=ADVANCED_FACE ( 'NONE', ( #50 ), #24882, .F. ) ;
#83313=CARTESIAN_POINT ( 'NONE',  ( -96.55620429048340725, -24.64898659630528499, 1.056161002820828143 ) ) ;
#83314=CARTESIAN_POINT ( 'NONE',  ( -45.62287095715004881, -25.00182538069145011, 7.747789668545099317 ) ) ;
#83315=CARTESIAN_POINT ( 'NONE',  ( -55.54039504408765993, -24.52300882791530157, 0.6510814631126364826 ) ) ;
#83317=DIRECTION ( 'NONE',  ( 0.000000000000000000, -0.9999999999976377785, -2.173523156925979128E-06 ) ) ;
#83318=EDGE_CURVE ( 'NONE', #54301, #1762, #72160, .T. ) ;
#83319=DIRECTION ( 'NONE',  ( -0.000000000000000000, 2.173523156925979552E-06, -0.9999999999976378895 ) ) ;
#83320=EDGE_CURVE ( 'NONE', #55337, #76238, #78238, .T. ) ;
#83321=LINE ( 'NONE', #37154, #68876 ) ;
#83322=CARTESIAN_POINT ( 'NONE',  ( 15.90762396150235958, 12.10710967819287198, 11.49999999999998934 ) ) ;
#83326=CARTESIAN_POINT ( 'NONE',  ( -45.57860638382562257, -24.83644354573578283, 8.397322867130103674 ) ) ;
#83328=CARTESIAN_POINT ( 'NONE',  ( -74.62287095715005592, -24.64898659630367561, 1.056161002820824368 ) ) ;
#83332=CARTESIAN_POINT ( 'NONE',  ( -36.52287095715006870, -29.50247984919015209, -1.443849546365060466 ) ) ;
#83334=CARTESIAN_POINT ( 'NONE',  ( -39.60068863268012507, -23.96119346886879597, -0.6495511937832143534 ) ) ;
#83335=B_SPLINE_CURVE_WITH_KNOTS ( 'NONE', 3,
 ( #43366, #83904, #14382, #61084, #59590, #20998 ),
 .UNSPECIFIED., .F., .F.,
 ( 4, 2, 4 ),
 ( 6.384118694779733475E-06, 0.001386860460836455327, 0.002767336802978130617 ),
 .UNSPECIFIED. ) ;
#83336=LINE ( 'NONE', #60024, #90201 ) ;
#83337=CARTESIAN_POINT ( 'NONE',  ( -51.69567503897438598, -25.31574286181298561, 4.127965101553169092 ) ) ;
#83338=DIRECTION ( 'NONE',  ( -3.773278334453079030E-23, 0.9999999999976377785, 2.173523156925979128E-06 ) ) ;
#83339=FACE_OUTER_BOUND ( 'NONE', #75010, .T. ) ;
#83341=CARTESIAN_POINT ( 'NONE',  ( -18.13051092187696156, -9.059970205480309957, -1.500000000000002220 ) ) ;
#83342=CARTESIAN_POINT ( 'NONE',  ( -122.5207654451141224, -23.96119346886880663, -0.6495511937832028071 ) ) ;
#83344=CARTESIAN_POINT ( 'NONE',  ( -109.6228709571501128, -23.94994826722516379, -0.6494450866351683116 ) ) ;
#83346=DIRECTION ( 'NONE',  ( -3.773278334453079618E-23, 0.9999999999976377785, 2.173523156925978705E-06 ) ) ;
#83347=CARTESIAN_POINT ( 'NONE',  ( -46.52287095715005449, -24.33927499327854349, 9.819080762295813614 ) ) ;
#83348=CARTESIAN_POINT ( 'NONE',  ( -15.22981678846565856, -13.14137338692033907, -1.500000000000002220 ) ) ;
#83349=CARTESIAN_POINT ( 'NONE',  ( -3.607955376466517095, 20.77440192976073519, 11.49999999999999645 ) ) ;
#83352=CARTESIAN_POINT ( 'NONE',  ( -70.63480130512397182, -24.52399227489126687, 9.353111116836529959 ) ) ;
#83353=CARTESIAN_POINT ( 'NONE',  ( 10.35204687333978057, 19.51823071965408829, 11.49999999999998934 ) ) ;
#83354=CARTESIAN_POINT ( 'NONE',  ( -20.18818894172909140, 3.697778396234267184, 11.49999999999998934 ) ) ;
#83355=LINE ( 'NONE', #20954, #30065 ) ;
#83358=ORIENTED_EDGE ( 'NONE', *, *, #56732, .T. ) ;
#83359=CARTESIAN_POINT ( 'NONE',  ( -99.12380231474227799, -25.27434709648489886, 4.001575133896465353 ) ) ;
#83361=CARTESIAN_POINT ( 'NONE',  ( -72.62287095715005592, -24.64965695001468404, 8.947790433994184056 ) ) ;
#83366=FACE_OUTER_BOUND ( 'NONE', #84109, .T. ) ;
#83367=CARTESIAN_POINT ( 'NONE',  ( 19.85042311639309531, 5.490197614093233369, -1.500000000000002220 ) ) ;
#83368=CARTESIAN_POINT ( 'NONE',  ( -4.019545577234938882, 21.20919285897865336, 11.49999999999999645 ) ) ;
#83369=VERTEX_POINT ( 'NONE', #40119 ) ;
#83370=DIRECTION ( 'NONE',  ( -3.773278334453079030E-23, 0.9999999999976377785, 2.173523156925979128E-06 ) ) ;
#83371=FACE_OUTER_BOUND ( 'NONE', #12117, .T. ) ;
#83372=CARTESIAN_POINT ( 'NONE',  ( 19.81157572017019319, -10.35993776028809421, -1.500000000000002220 ) ) ;
#83373=CARTESIAN_POINT ( 'NONE',  ( -48.62287095715004881, -23.48786465467241058, 11.44779295918254824 ) ) ;
#83375=ORIENTED_EDGE ( 'NONE', *, *, #41255, .F. ) ;
#83377=CARTESIAN_POINT ( 'NONE',  ( -49.63342129923848489, -24.35071581493542325, 9.817618358456035921 ) ) ;
#83378=B_SPLINE_CURVE_WITH_KNOTS ( 'NONE', 3,
 ( #32177, #64164, #95085, #25570 ),
 .UNSPECIFIED., .F., .F.,
 ( 4, 4 ),
 ( 0.000000000000000000, 0.0001000000000000028644 ),
 .UNSPECIFIED. ) ;
#83379=CARTESIAN_POINT ( 'NONE',  ( 18.69404101259207707, 9.334567778723176446, 11.49999999999998934 ) ) ;
#83380=VERTEX_POINT ( 'NONE', #92390 ) ;
#83383=CARTESIAN_POINT ( 'NONE',  ( -86.59502635198218456, -23.96119346886881019, -0.6495511937831902616 ) ) ;
#83385=VERTEX_POINT ( 'NONE', #30995 ) ;
#83386=CARTESIAN_POINT ( 'NONE',  ( -100.5064008495685357, -24.83644354573578994, 8.397322867130101898 ) ) ;
#83387=CARTESIAN_POINT ( 'NONE',  ( 13.68530018921192060, -16.06810839794082924, -1.500000000000002220 ) ) ;
#83391=FACE_OUTER_BOUND ( 'NONE', #29438, .T. ) ;
#83392=CARTESIAN_POINT ( 'NONE',  ( 21.36706796925463792, 4.321743776461201669, -1.500000000000002220 ) ) ;
#83393=CARTESIAN_POINT ( 'NONE',  ( -110.9909297185884327, -25.14264188228929697, 6.986250900936915365 ) ) ;
#83394=CARTESIAN_POINT ( 'NONE',  ( -36.62287095715004170, -23.94994826722565406, -0.6494450866342751372 ) ) ;
#83395=CARTESIAN_POINT ( 'NONE',  ( -84.58953762381672448, -24.64965694238407679, 8.947790433994653014 ) ) ;
#83396=CARTESIAN_POINT ( 'NONE',  ( 20.88924836996103451, 6.054424527964996194, -1.500000000000002220 ) ) ;
#83397=CARTESIAN_POINT ( 'NONE',  ( -71.53293015653792963, -25.31639593012666012, 5.453599084002859421 ) ) ;
#83398=CARTESIAN_POINT ( 'NONE',  ( -2.124831620219566730, 22.23837930986240607, 11.49999999999999645 ) ) ;
#83399=EDGE_LOOP ( 'NONE', ( #97835, #43352, #87160, #87871 ) ) ;
#83400=CARTESIAN_POINT ( 'NONE',  ( -45.62287095715007013, -24.63287334234178871, 0.9662140553045390767 ) ) ;
#83401=CARTESIAN_POINT ( 'NONE',  ( -69.62287095715005592, -23.47596703998600631, 11.44779298504227683 ) ) ;
#83404=VECTOR ( 'NONE', #81389, 1000.000000000000114 ) ;
#83406=ORIENTED_EDGE ( 'NONE', *, *, #54621, .T. ) ;
#83407=CARTESIAN_POINT ( 'NONE',  ( -75.52287095715013265, -23.85196035786901447, -0.8779234886475122401 ) ) ;
#83409=CARTESIAN_POINT ( 'NONE',  ( -52.52287095715006870, -23.48786465467241058, 11.44779295918255002 ) ) ;
#83410=CARTESIAN_POINT ( 'NONE',  ( -49.10457154551149728, -25.27419814425984512, 3.999772249604824914 ) ) ;
#83412=CARTESIAN_POINT ( 'NONE',  ( -37.62287095715003460, -23.73934037231756378, 11.05740245334329863 ) ) ;
#83413=CARTESIAN_POINT ( 'NONE',  ( -45.62287095715004881, -23.47596703998600276, 11.44779298504227505 ) ) ;
#83415=CARTESIAN_POINT ( 'NONE',  ( -18.22486019313910077, 6.713856318530649681, 11.49999999999999645 ) ) ;
#83416=CARTESIAN_POINT ( 'NONE',  ( -87.92287095715006728, -23.47596703998600631, 11.44779298504227860 ) ) ;
#83417=VERTEX_POINT ( 'NONE', #7155 ) ;
#83420=CARTESIAN_POINT ( 'NONE',  ( -116.5228709571501042, -23.47593901973090524, -1.443836447538996426 ) ) ;
#83421=CARTESIAN_POINT ( 'NONE',  ( -65.62287095715005592, -29.50250786944525672, 11.44777988621623699 ) ) ;
#83422=EDGE_CURVE ( 'NONE', #20204, #39807, #58864, .T. ) ;
#83423=CARTESIAN_POINT ( 'NONE',  ( -19.07250549579359244, -4.594354733287289605, -1.500000000000002220 ) ) ;
#83425=ORIENTED_EDGE ( 'NONE', *, *, #10972, .F. ) ;
#83427=CARTESIAN_POINT ( 'NONE',  ( 0.7969447072908428797, -21.54811710690876225, 11.49999999999998934 ) ) ;
#83429=CARTESIAN_POINT ( 'NONE',  ( -70.61198345729647485, -25.12219137084317211, 7.066382252255097640 ) ) ;
#83430=CARTESIAN_POINT ( 'NONE',  ( -50.52287095715008292, -24.62226745350441703, 0.9660975649729551806 ) ) ;
#83431=B_SPLINE_CURVE_WITH_KNOTS ( 'NONE', 3,
 ( #98179, #83960, #6830, #14440, #45412, #76335 ),
 .UNSPECIFIED., .F., .F.,
 ( 4, 2, 4 ),
 ( 0.000000000000000000, 0.001380764517854763665, 0.002761529035709527329 ),
 .UNSPECIFIED. ) ;
#83432=CARTESIAN_POINT ( 'NONE',  ( -99.72418814851606328, -25.18439392545337796, 3.555267871858176942 ) ) ;
#83433=CARTESIAN_POINT ( 'NONE',  ( 3.314627170985911420, 22.80399709308638023, -1.500000000000002220 ) ) ;
#83436=DIRECTION ( 'NONE',  ( -3.773278334453079030E-23, 0.9999999999976377785, 2.173523156925979128E-06 ) ) ;
#83437=CARTESIAN_POINT ( 'NONE',  ( 14.76687977769557847, -13.71354340032049457, 11.49999999999999645 ) ) ;
#83438=CARTESIAN_POINT ( 'NONE',  ( -84.62287095715008434, -23.47596703998600631, 11.44779298504227860 ) ) ;
#83439=CARTESIAN_POINT ( 'NONE',  ( -52.52287095715006870, -29.50248528299804818, 1.056150453629033370 ) ) ;
#83440=ADVANCED_FACE ( 'NONE', ( #38106 ), #26396, .T. ) ;
#83442=CARTESIAN_POINT ( 'NONE',  ( -29.62287095715004881, -23.40875089534885589, 11.44779299594469713 ) ) ;
#83443=CARTESIAN_POINT ( 'NONE',  ( -122.5228709571500048, -23.73934037231757443, 11.05740245334328087 ) ) ;
#83444=CARTESIAN_POINT ( 'NONE',  ( -6.239078800006583769, 18.87631364486404806, -1.500000000000002220 ) ) ;
#83445=ADVANCED_FACE ( 'NONE', ( #33011 ), #25892, .F. ) ;
#83446=CARTESIAN_POINT ( 'NONE',  ( -113.5541410105945488, -24.15543982623907482, -0.2315651400026574047 ) ) ;
#83447=CARTESIAN_POINT ( 'NONE',  ( 11.81298147481671279, -15.83112273922526470, -1.500000000000002220 ) ) ;
#83449=EDGE_CURVE ( 'NONE', #5568, #64035, #87796, .T. ) ;
#83451=CARTESIAN_POINT ( 'NONE',  ( -78.62287095715004170, -23.48786465467241413, 11.44779295918254469 ) ) ;
#83452=CARTESIAN_POINT ( 'NONE',  ( -74.62287095715005592, -23.47596703998600631, 11.44779298504227860 ) ) ;
#83453=CARTESIAN_POINT ( 'NONE',  ( -3.285303218690974525, -20.39892020120133154, 11.49999999999999645 ) ) ;
#83454=CARTESIAN_POINT ( 'NONE',  ( -70.62287095715005592, -23.47593901973091235, -1.443836447539006196 ) ) ;
#83455=ADVANCED_FACE ( 'NONE', ( #88803 ), #25389, .T. ) ;
#83457=CARTESIAN_POINT ( 'NONE',  ( -106.5596206104284533, -23.48783264082477373, -1.443836473390085695 ) ) ;
#83458=CARTESIAN_POINT ( 'NONE',  ( -13.93578158028743985, 17.96481793202167054, 11.49999999999999645 ) ) ;
#83459=ORIENTED_EDGE ( 'NONE', *, *, #13599, .F. ) ;
#83461=CARTESIAN_POINT ( 'NONE',  ( -62.55620429048339304, -23.47593901973091235, -1.443836447539007972 ) ) ;
#83462=CARTESIAN_POINT ( 'NONE',  ( 8.007726535620864894, 18.53121347637897287, 11.49999999999998934 ) ) ;
#83463=EDGE_CURVE ( 'NONE', #15126, #98224, #18281, .T. ) ;
#83464=CARTESIAN_POINT ( 'NONE',  ( -63.53936857308043074, -24.51314013834316796, 0.6176544820404160641 ) ) ;
#83467=ORIENTED_EDGE ( 'NONE', *, *, #3097, .F. ) ;
#83469=ORIENTED_EDGE ( 'NONE', *, *, #58494, .F. ) ;
#83471=CARTESIAN_POINT ( 'NONE',  ( 21.34038654641452482, 8.310931564070170197, -1.500000000000002220 ) ) ;
#83472=CARTESIAN_POINT ( 'NONE',  ( -29.48132452782988366, -24.42614700373432512, 0.6176547996449994749 ) ) ;
#83473=CARTESIAN_POINT ( 'NONE',  ( -21.33164055427280914, -3.227942221655450972, -1.500000000000002220 ) ) ;
#83474=DIRECTION ( 'NONE',  ( -3.773278334453079030E-23, 0.9999999999976377785, 2.173523156925979128E-06 ) ) ;
#83476=CARTESIAN_POINT ( 'NONE',  ( 5.579783289733251550, -20.15082174716252794, 11.49999999999999645 ) ) ;
#83477=VERTEX_POINT ( 'NONE', #96903 ) ;
#83478=CARTESIAN_POINT ( 'NONE',  ( -50.52287095715006160, -23.47596703998600631, 11.44779298504229104 ) ) ;
#83479=CARTESIAN_POINT ( 'NONE',  ( 12.33731239738771102, -18.22686410513083288, 11.49999999999998934 ) ) ;
#83480=CARTESIAN_POINT ( 'NONE',  ( -105.6242952428360127, -24.92592662359561473, 8.075495903017998245 ) ) ;
#83481=CARTESIAN_POINT ( 'NONE',  ( -27.89469851781394283, -25.21724992210043581, 7.595245531572402342 ) ) ;
#83482=ORIENTED_EDGE ( 'NONE', *, *, #15907, .F. ) ;
#83484=CARTESIAN_POINT ( 'NONE',  ( -90.54594762189722701, -24.63419186844611275, 9.035850630976923981 ) ) ;
#83485=B_SPLINE_CURVE_WITH_KNOTS ( 'NONE', 3,
 ( #81584, #17679, #11068, #50629 ),
 .UNSPECIFIED., .F., .F.,
 ( 4, 4 ),
 ( 0.000000000000000000, 0.0005192307692307995826 ),
 .UNSPECIFIED. ) ;
#83487=CARTESIAN_POINT ( 'NONE',  ( -72.64441443556766842, -23.73791477778911840, 11.05961554403170943 ) ) ;
#83488=ORIENTED_EDGE ( 'NONE', *, *, #61215, .T. ) ;
#83489=B_SPLINE_CURVE_WITH_KNOTS ( 'NONE', 3,
 ( #58104, #89533, #89039, #96154 ),
 .UNSPECIFIED., .F., .F.,
 ( 4, 4 ),
 ( 0.9411720679360631170, 0.9501784992081787617 ),
 .UNSPECIFIED. ) ;
#83490=ORIENTED_EDGE ( 'NONE', *, *, #30978, .F. ) ;
#83491=CARTESIAN_POINT ( 'NONE',  ( -40.49165087243459737, -25.29352311369862605, 5.543942880681965946 ) ) ;
#83492=CARTESIAN_POINT ( 'NONE',  ( -92.52287095715006160, -29.50248528299804818, 1.056150453629040253 ) ) ;
#83493=CARTESIAN_POINT ( 'NONE',  ( -36.56104621580127656, -23.73766607897670156, -1.055555164236459120 ) ) ;
#83494=CARTESIAN_POINT ( 'NONE',  ( 2.554409723529738052, 20.22502395925995700, -1.500000000000002220 ) ) ;
#83495=EDGE_CURVE ( 'NONE', #73557, #33030, #64489, .T. ) ;
#83496=ORIENTED_EDGE ( 'NONE', *, *, #96739, .T. ) ;
#83498=CARTESIAN_POINT ( 'NONE',  ( -30.62155233649869146, -24.14929313691197876, 10.49653219292474482 ) ) ;
#83499=EDGE_CURVE ( 'NONE', #3731, #49859, #41993, .T. ) ;
#83501=CARTESIAN_POINT ( 'NONE',  ( -25.56006801123770700, -24.90049575466193232, 5.680075578843891471 ) ) ;
#83503=DIRECTION ( 'NONE',  ( -0.000000000000000000, 2.173523156925979552E-06, -0.9999999999976378895 ) ) ;
#83504=CARTESIAN_POINT ( 'NONE',  ( -29.31102972132424966, -25.26247878080915399, 7.337442809714779024 ) ) ;
#83506=CARTESIAN_POINT ( 'NONE',  ( 6.705275102110877405, 19.67741782454948662, 11.49999999999998934 ) ) ;
#83507=ORIENTED_EDGE ( 'NONE', *, *, #42824, .F. ) ;
#83510=ORIENTED_EDGE ( 'NONE', *, *, #42921, .T. ) ;
#83513=EDGE_LOOP ( 'NONE', ( #71930, #48499, #7897, #52431 ) ) ;
#83516=CARTESIAN_POINT ( 'NONE',  ( -50.55649023882089921, -25.27412228879126133, 2.837765180535595011 ) ) ;
#83518=CARTESIAN_POINT ( 'NONE',  ( -86.52287095715007581, -24.50216790748203977, 0.6166512839542572788 ) ) ;
#83519=LINE ( 'NONE', #52582, #80500 ) ;
#83520=CARTESIAN_POINT ( 'NONE',  ( -22.05048665130746954, -1.834114841651104832, 11.49999999999999645 ) ) ;
#83522=CARTESIAN_POINT ( 'NONE',  ( -108.5181468800120399, -23.96119346886881729, -0.6495511937831862648 ) ) ;
#83523=CARTESIAN_POINT ( 'NONE',  ( 20.10346781357453949, 10.43426432342431553, 11.49999999999998934 ) ) ;
#83526=B_SPLINE_CURVE_WITH_KNOTS ( 'NONE', 3,
 ( #15663, #8560, #45625, #14155 ),
 .UNSPECIFIED., .F., .F.,
 ( 4, 4 ),
 ( 0.000000000000000000, 9.999999999998897304E-05 ),
 .UNSPECIFIED. ) ;
#83528=CARTESIAN_POINT ( 'NONE',  ( -29.52287095715006515, -23.38906523657919578, -1.443836447538998424 ) ) ;
#83529=B_SPLINE_CURVE_WITH_KNOTS ( 'NONE', 3,
 ( #25414, #70591, #88321, #48771, #79697, #1591 ),
 .UNSPECIFIED., .F., .F.,
 ( 4, 2, 4 ),
 ( 6.391158118959990520E-06, 0.001387004593080781809, 0.002767618028042603730 ),
 .UNSPECIFIED. ) ;
#83530=VECTOR ( 'NONE', #19051, 1000.000000000000114 ) ;
#83533=CARTESIAN_POINT ( 'NONE',  ( -17.82723130383223165, -9.322377578706960932, 11.49999999999998934 ) ) ;
#83535=ORIENTED_EDGE ( 'NONE', *, *, #83242, .T. ) ;
#83536=CARTESIAN_POINT ( 'NONE',  ( -89.52287095715006160, -23.48786465467241769, 11.44779295918254292 ) ) ;
#83537=CARTESIAN_POINT ( 'NONE',  ( -16.35649155429130985, -15.18990082740072367, -1.500000000000002220 ) ) ;
#83540=ORIENTED_EDGE ( 'NONE', *, *, #16038, .F. ) ;
#83541=VERTEX_POINT ( 'NONE', #73573 ) ;
#83542=CARTESIAN_POINT ( 'NONE',  ( -110.6228709571500701, -23.48786465467241769, 11.44779295918254114 ) ) ;
#83548=CARTESIAN_POINT ( 'NONE',  ( -5.499840656826012975, 18.73951620154120334, 11.49999999999998934 ) ) ;
#83550=CARTESIAN_POINT ( 'NONE',  ( -10.41973078503355588, 18.78793304046337198, -1.500000000000002220 ) ) ;
#83552=LINE ( 'NONE', #13534, #84308 ) ;
#83554=CARTESIAN_POINT ( 'NONE',  ( -6.082769120682566921, -21.99330073093985405, -1.500000000000002220 ) ) ;
#83555=CARTESIAN_POINT ( 'NONE',  ( -96.63021412912847552, -24.15620529776628445, 10.23563542870660115 ) ) ;
#83556=CARTESIAN_POINT ( 'NONE',  ( -127.6228709571500559, -23.47593901973091235, -1.443836447538995760 ) ) ;
#83557=CARTESIAN_POINT ( 'NONE',  ( 15.90762396150235958, 12.10710967819287198, 11.49999999999999645 ) ) ;
#83558=CARTESIAN_POINT ( 'NONE',  ( -64.58953762381673869, -24.64898659630528499, 1.056161002820823036 ) ) ;
#83559=CARTESIAN_POINT ( 'NONE',  ( -74.60134804213069515, -23.73791477778911840, 11.05961554403170588 ) ) ;
#83563=DIRECTION ( 'NONE',  ( 0.000000000000000000, -2.173523156925980399E-06, 0.9999999999976378895 ) ) ;
#83565=CARTESIAN_POINT ( 'NONE',  ( 18.95625057990686813, 10.65820999021175730, 11.49999999999998934 ) ) ;
#83567=CARTESIAN_POINT ( 'NONE',  ( -11.98250242409135780, 15.54504917500377559, -1.500000000000002220 ) ) ;
#83568=CARTESIAN_POINT ( 'NONE',  ( -99.36303409631229044, -25.22482018454191888, 6.487150432439984904 ) ) ;
#83569=ORIENTED_EDGE ( 'NONE', *, *, #46466, .F. ) ;
#83573=DIRECTION ( 'NONE',  ( -3.773278334444167608E-23, 1.000000000000000000, 0.000000000000000000 ) ) ;
#83575=CARTESIAN_POINT ( 'NONE',  ( -7.951223608505463503, 18.87544906973805325, 11.49999999999999645 ) ) ;
#83577=EDGE_CURVE ( 'NONE', #62364, #80236, #81179, .T. ) ;
#83578=CARTESIAN_POINT ( 'NONE',  ( -88.52287095715006160, -23.47596703998600631, 11.44779298504228393 ) ) ;
#83579=ORIENTED_EDGE ( 'NONE', *, *, #59491, .F. ) ;
#83581=CARTESIAN_POINT ( 'NONE',  ( -39.74201634257447324, -25.28892478847090430, 3.555061831638682168 ) ) ;
#83582=LINE ( 'NONE', #14574, #3076 ) ;
#83583=EDGE_CURVE ( 'NONE', #53349, #27745, #2072, .T. ) ;
#83584=CARTESIAN_POINT ( 'NONE',  ( -85.52287095715006160, -23.48783264082476663, -1.443836473390089470 ) ) ;
#83587=CARTESIAN_POINT ( 'NONE',  ( -13.34915495237762251, 18.83725853537101358, 11.49999999999999645 ) ) ;
#83588=CARTESIAN_POINT ( 'NONE',  ( -13.73562189146022661, -18.16285900770654393, -1.500000000000002220 ) ) ;
#83590=CARTESIAN_POINT ( 'NONE',  ( -105.6228709571500843, -24.14321612903118464, -0.2833117244520867439 ) ) ;
#83591=DIRECTION ( 'NONE',  ( 0.000000000000000000, -2.173523156925980399E-06, 0.9999999999976378895 ) ) ;
#83592=CARTESIAN_POINT ( 'NONE',  ( -74.52287095715004739, -24.51387760970726148, 9.387446482453416507 ) ) ;
#83593=CARTESIAN_POINT ( 'NONE',  ( -99.50663065733192525, -25.30157701748021637, 4.996268205051663358 ) ) ;
#83594=CARTESIAN_POINT ( 'NONE',  ( -0.1377007522546883911, -21.91379463844567965, -1.500000000000002220 ) ) ;
#83596=VECTOR ( 'NONE', #5479, 1000.000000000000114 ) ;
#83599=CARTESIAN_POINT ( 'NONE',  ( -77.62287095715005592, -23.96127896941631619, -0.6493128931037820406 ) ) ;
#83602=CARTESIAN_POINT ( 'NONE',  ( -107.6228709571500985, -23.95044443724993144, 10.65354141964649592 ) ) ;
#83605=CARTESIAN_POINT ( 'NONE',  ( -3.558151220431595707, 20.12126150705307381, 11.49999999999998934 ) ) ;
#83608=ORIENTED_EDGE ( 'NONE', *, *, #37342, .F. ) ;
#83609=VERTEX_POINT ( 'NONE', #17785 ) ;
#83610=ORIENTED_EDGE ( 'NONE', *, *, #19817, .F. ) ;
#83612=CARTESIAN_POINT ( 'NONE',  ( -22.90524134523018773, 2.401388714834002069, 11.49999999999998934 ) ) ;
#83613=CARTESIAN_POINT ( 'NONE',  ( -35.52287095715008292, -24.92579138211052481, 1.929029949967122182 ) ) ;
#83614=B_SPLINE_CURVE_WITH_KNOTS ( 'NONE', 3,
 ( #5082, #19798, #28411, #50773, #81714, #36526 ),
 .UNSPECIFIED., .F., .F.,
 ( 4, 2, 4 ),
 ( 6.391158118972359742E-06, 0.001387004593080795036, 0.002767618028042617608 ),
 .UNSPECIFIED. ) ;
#83615=CARTESIAN_POINT ( 'NONE',  ( -5.512817753899047268, 19.46650688538001361, -1.500000000000002220 ) ) ;
#83616=VECTOR ( 'NONE', #99014, 1000.000000000000114 ) ;
#83621=EDGE_CURVE ( 'NONE', #71750, #10167, #21276, .T. ) ;
#83622=CARTESIAN_POINT ( 'NONE',  ( -128.2228709571500644, -23.47596703998600631, 11.44779298504227860 ) ) ;
#83623=CARTESIAN_POINT ( 'NONE',  ( -99.59346001018235484, -23.96169478059713498, 10.65365249895717703 ) ) ;
#83624=CARTESIAN_POINT ( 'NONE',  ( -8.434714792116727367, -19.68496499552307455, 11.49999999999999645 ) ) ;
#83625=ORIENTED_EDGE ( 'NONE', *, *, #54736, .F. ) ;
#83626=DIRECTION ( 'NONE',  ( -3.773278334444167608E-23, 1.000000000000000000, 0.000000000000000000 ) ) ;
#83627=CARTESIAN_POINT ( 'NONE',  ( -94.52287095715009002, -23.73934037231757443, 11.05740245334328087 ) ) ;
#83628=VERTEX_POINT ( 'NONE', #51230 ) ;
#83629=CARTESIAN_POINT ( 'NONE',  ( -20.69558417703438025, 1.077208295497980250, 11.49999999999998934 ) ) ;
#83634=CARTESIAN_POINT ( 'NONE',  ( -28.62974205479175893, -24.36036647229939334, 0.6176551810875500204 ) ) ;
#83638=CARTESIAN_POINT ( 'NONE',  ( -1.027814097295878693, -20.98676634966329146, -1.500000000000002220 ) ) ;
#83639=CARTESIAN_POINT ( 'NONE',  ( 21.83198049998918577, 2.282343850347359648, 11.49999999999999645 ) ) ;
#83640=CARTESIAN_POINT ( 'NONE',  ( -37.64193247772556816, -24.15620529776627379, 10.23563542870660825 ) ) ;
#83641=CARTESIAN_POINT ( 'NONE',  ( 13.09772080625096891, 18.35129493929886380, 11.49999999999998934 ) ) ;
#83642=AXIS2_PLACEMENT_3D ( 'NONE', #93526, #14903, #91537 ) ;
#83643=CARTESIAN_POINT ( 'NONE',  ( -9.893913718187896222, 18.50344063021147889, -1.500000000000002220 ) ) ;
#83645=LINE ( 'NONE', #52708, #48633 ) ;
#83647=ORIENTED_EDGE ( 'NONE', *, *, #52855, .F. ) ;
#83648=ORIENTED_EDGE ( 'NONE', *, *, #94324, .F. ) ;
#83649=ORIENTED_EDGE ( 'NONE', *, *, #43655, .T. ) ;
#83650=CARTESIAN_POINT ( 'NONE',  ( -68.52287095715007581, -23.47593901973090524, -1.443836447538997092 ) ) ;
#83652=CARTESIAN_POINT ( 'NONE',  ( 4.075586527997184128, 21.15050231453075824, -1.500000000000002220 ) ) ;
#83653=FACE_OUTER_BOUND ( 'NONE', #39643, .T. ) ;
#83654=ORIENTED_EDGE ( 'NONE', *, *, #54633, .F. ) ;
#83655=CARTESIAN_POINT ( 'NONE',  ( 6.686094007546604878, -20.02240253118446844, 11.49999999999998934 ) ) ;
#83656=LINE ( 'NONE', #76530, #1197 ) ;
#83657=CARTESIAN_POINT ( 'NONE',  ( -64.60983413518364671, -23.48783264082477018, -1.443836473390096353 ) ) ;
#83658=EDGE_CURVE ( 'NONE', #4528, #39813, #45566, .T. ) ;
#83659=CARTESIAN_POINT ( 'NONE',  ( -83.54730440395789515, -24.35071581493543036, 9.817618358456028815 ) ) ;
#83660=DIRECTION ( 'NONE',  ( -3.773278334453079618E-23, 0.9999999999976377785, 2.173523156925979975E-06 ) ) ;
#83661=CARTESIAN_POINT ( 'NONE',  ( -70.74026866089610621, -25.31511106678998502, 4.894904372220056921 ) ) ;
#83662=CARTESIAN_POINT ( 'NONE',  ( 22.15222936869060177, 0.07132910108538677296, -1.500000000000002220 ) ) ;
#83666=CARTESIAN_POINT ( 'NONE',  ( -59.52287095715006160, -23.47596703998600631, 11.44779298504228926 ) ) ;
#83668=EDGE_CURVE ( 'NONE', #93720, #22199, #36494, .T. ) ;
#83669=ADVANCED_FACE ( 'NONE', ( #52728 ), #32139, .T. ) ;
#83672=CARTESIAN_POINT ( 'NONE',  ( 19.43689267596983683, 0.5339526363925560792, 11.49999999999998934 ) ) ;
#83673=CARTESIAN_POINT ( 'NONE',  ( 3.659817510876246960, 21.07357064420920878, -1.500000000000002220 ) ) ;
#83674=CARTESIAN_POINT ( 'NONE',  ( -62.49492364790526722, -24.51314013834316441, 0.6176544820404141767 ) ) ;
#83676=CARTESIAN_POINT ( 'NONE',  ( -117.6228709571500701, -24.66019654487199730, 8.947790411086121054 ) ) ;
#83677=CARTESIAN_POINT ( 'NONE',  ( -36.62287095715007013, -23.73934037231756378, 11.05740245334329863 ) ) ;
#83678=CARTESIAN_POINT ( 'NONE',  ( 2.978076788109338402, -22.46882643481310282, -1.500000000000002220 ) ) ;
#83681=CARTESIAN_POINT ( 'NONE',  ( -128.6228709571500417, -24.65952944569305316, 1.056160979905707897 ) ) ;
#83682=CARTESIAN_POINT ( 'NONE',  ( -122.6228709571500701, -23.48783264082479505, -1.443836473390058828 ) ) ;
#83683=CARTESIAN_POINT ( 'NONE',  ( 19.60560811685724403, 2.727087469661350738, 11.49999999999999645 ) ) ;
#83687=ORIENTED_EDGE ( 'NONE', *, *, #37014, .T. ) ;
#83688=CARTESIAN_POINT ( 'NONE',  ( -53.62287095715005592, -23.47596703998600276, 11.44779298504227683 ) ) ;
#83690=CARTESIAN_POINT ( 'NONE',  ( 3.837509532605410278, -21.31939230324424628, -1.500000000000002220 ) ) ;
#83691=DIRECTION ( 'NONE',  ( -3.773278334453079618E-23, 0.9999999999976377785, 2.173523156925979975E-06 ) ) ;
#83692=CARTESIAN_POINT ( 'NONE',  ( 14.41255161864883583, -12.98630880007775268, -1.500000000000002220 ) ) ;
#83694=CARTESIAN_POINT ( 'NONE',  ( -61.62287095715004881, -23.48783264082478439, -1.443836473390069042 ) ) ;
#83695=CARTESIAN_POINT ( 'NONE',  ( -35.62287095715004881, -24.52232992886363050, 0.6492154411906073674 ) ) ;
#83696=CARTESIAN_POINT ( 'NONE',  ( 19.75791096855702733, 1.210928449428283038, -1.500000000000002220 ) ) ;
#83698=CARTESIAN_POINT ( 'NONE',  ( -18.23349369547262810, -8.965252873808195133, 11.49999999999999645 ) ) ;
#83699=CARTESIAN_POINT ( 'NONE',  ( -80.57997298781928919, -25.00158670708910691, 2.256160236439221034 ) ) ;
#83704=CARTESIAN_POINT ( 'NONE',  ( -0.1426030150137700958, -21.20389190742571373, -1.497999999999532816 ) ) ;
#83705=DIRECTION ( 'NONE',  ( -3.773278334453080206E-23, 0.9999999999976377785, 2.173523156925979552E-06 ) ) ;
#83707=CARTESIAN_POINT ( 'NONE',  ( -95.62287095715009855, -24.83602698348160587, 1.605859176311266179 ) ) ;
#83708=DIRECTION ( 'NONE',  ( -3.773278334453080206E-23, 0.9999999999976377785, 2.173523156925979975E-06 ) ) ;
#83709=CARTESIAN_POINT ( 'NONE',  ( -13.75281105048956576, 14.62798779934380811, -1.500000000000002220 ) ) ;
#83710=EDGE_CURVE ( 'NONE', #8399, #64351, #57611, .T. ) ;
#83711=CARTESIAN_POINT ( 'NONE',  ( -85.52287095715004739, -24.99132157543166954, 2.256160258750667502 ) ) ;
#83712=ORIENTED_EDGE ( 'NONE', *, *, #95965, .F. ) ;
#83714=AXIS2_PLACEMENT_3D ( 'NONE', #89247, #81635, #19715 ) ;
#83717=CARTESIAN_POINT ( 'NONE',  ( -22.76716317511769461, -1.676022972194794791, 11.49999999999999645 ) ) ;
#83718=DIRECTION ( 'NONE',  ( 0.000000000000000000, 0.9999999999976377785, 2.173523156925979552E-06 ) ) ;
#83720=CARTESIAN_POINT ( 'NONE',  ( -114.5228709571500616, -24.65952944569305316, 1.056160979905704123 ) ) ;
#83723=CARTESIAN_POINT ( 'NONE',  ( -95.62287095715005592, -29.50250786944525672, 11.44777988621623166 ) ) ;
#83724=CARTESIAN_POINT ( 'NONE',  ( -108.6228709571500417, -24.65952944569305316, 1.056160979905705011 ) ) ;
#83725=ORIENTED_EDGE ( 'NONE', *, *, #54638, .F. ) ;
#83726=CARTESIAN_POINT ( 'NONE',  ( 20.12614038868121824, 2.982395457389826809, 11.49999999999998934 ) ) ;
#83727=ORIENTED_EDGE ( 'NONE', *, *, #56281, .F. ) ;
#83728=CARTESIAN_POINT ( 'NONE',  ( 22.85142058292489153, -2.183311388647848350, -1.500000000000002220 ) ) ;
#83730=EDGE_LOOP ( 'NONE', ( #68754, #58759, #68488, #91842 ) ) ;
#83731=CARTESIAN_POINT ( 'NONE',  ( -38.62287095715005592, -23.72747288104442021, -1.053458166803663554 ) ) ;
#83733=CARTESIAN_POINT ( 'NONE',  ( -77.59611031647311563, -23.96169478059713498, 10.65365249895717703 ) ) ;
#83734=CARTESIAN_POINT ( 'NONE',  ( -51.56024044797280226, -23.73791477778911840, 11.05961554403170766 ) ) ;
#83735=CARTESIAN_POINT ( 'NONE',  ( -13.59518820711925358, -16.35513075224449864, 11.49999999999999645 ) ) ;
#83736=ORIENTED_EDGE ( 'NONE', *, *, #93681, .T. ) ;
#83738=CARTESIAN_POINT ( 'NONE',  ( 19.92104321119709098, 9.795001720801039369, -1.500000000000002220 ) ) ;
#83739=CARTESIAN_POINT ( 'NONE',  ( -7.658335995763069448, 19.15843701367676388, 11.49999999999998934 ) ) ;
#83742=ORIENTED_EDGE ( 'NONE', *, *, #76787, .F. ) ;
#83747=AXIS2_PLACEMENT_3D ( 'NONE', #64720, #18505, #96142 ) ;
#83748=ORIENTED_EDGE ( 'NONE', *, *, #38257, .T. ) ;
#83749=CARTESIAN_POINT ( 'NONE',  ( -126.3656746162385645, -25.21753786267799313, 3.540021004441403996 ) ) ;
#83751=CARTESIAN_POINT ( 'NONE',  ( -19.76906661924035191, -6.534152953431121347, -1.500000000000002220 ) ) ;
#83752=CARTESIAN_POINT ( 'NONE',  ( 21.79142754302170815, -0.6654467836950721527, 11.49999999999999645 ) ) ;
#83753=CARTESIAN_POINT ( 'NONE',  ( -51.07287736509689324, -25.05542596678760603, 7.456204470533294604 ) ) ;
#83754=CARTESIAN_POINT ( 'NONE',  ( -78.59598984800533117, -23.96169478059713498, 10.65365249895717881 ) ) ;
#83755=CARTESIAN_POINT ( 'NONE',  ( 15.63351008929417318, -16.12541905121107177, -1.500000000000002220 ) ) ;
#83756=VECTOR ( 'NONE', #66611, 1000.000000000000114 ) ;
#83757=B_SPLINE_CURVE_WITH_KNOTS ( 'NONE', 3,
 ( #91771, #98384, #59852, #82670 ),
 .UNSPECIFIED., .F., .F.,
 ( 4, 4 ),
 ( 0.02980720907600921399, 0.03881364034812469915 ),
 .UNSPECIFIED. ) ;
#83764=FACE_OUTER_BOUND ( 'NONE', #42882, .T. ) ;
#83765=EDGE_LOOP ( 'NONE', ( #43864, #57655, #22575, #82627 ) ) ;
#83767=CARTESIAN_POINT ( 'NONE',  ( -16.81368161134402683, 13.12552177539105358, -1.500000000000002220 ) ) ;
#83768=ORIENTED_EDGE ( 'NONE', *, *, #26761, .T. ) ;
#83770=CARTESIAN_POINT ( 'NONE',  ( -11.20027426441765961, 17.80179601997297212, 11.49999999999998934 ) ) ;
#83771=CARTESIAN_POINT ( 'NONE',  ( -30.61204402015759740, -24.38902418599227673, 0.3015907515355735202 ) ) ;
#83772=CARTESIAN_POINT ( 'NONE',  ( -113.5228709571500616, -24.64965694238408034, 8.947790433994192938 ) ) ;
#83773=DIRECTION ( 'NONE',  ( -3.773278334453080206E-23, 0.9999999999976377785, 2.173523156925979975E-06 ) ) ;
#83774=CARTESIAN_POINT ( 'NONE',  ( 11.09338859787202480, -18.89396691112096605, -1.500000000000002220 ) ) ;
#83777=CARTESIAN_POINT ( 'NONE',  ( -122.5190326059218933, -24.51419770103158413, 9.386484678747169852 ) ) ;
#83779=AXIS2_PLACEMENT_3D ( 'NONE', #55591, #70808, #63716 ) ;
#83780=EDGE_CURVE ( 'NONE', #24356, #54444, #23804, .T. ) ;
#83782=CARTESIAN_POINT ( 'NONE',  ( -120.5228709571500900, -24.14321612903119885, -0.2833117244520856892 ) ) ;
#83783=CARTESIAN_POINT ( 'NONE',  ( -130.5728709571500588, -23.78087380709146004, 10.97511746239721298 ) ) ;
#83784=EDGE_CURVE ( 'NONE', #57062, #884, #65366, .T. ) ;
#83786=CARTESIAN_POINT ( 'NONE',  ( -10.25202023458897393, -22.90670518572982672, 9.440663514584137772 ) ) ;
#83787=CARTESIAN_POINT ( 'NONE',  ( 12.11089201280794470, -17.53110042540249225, 11.49999999999998934 ) ) ;
#83788=CARTESIAN_POINT ( 'NONE',  ( -112.5587146430100489, -23.48783264082478794, -1.443836473390061270 ) ) ;
#83789=CARTESIAN_POINT ( 'NONE',  ( -27.68651082257923335, -24.97064402014857620, 2.274902934185277559 ) ) ;
#83791=CARTESIAN_POINT ( 'NONE',  ( -100.6814946224345846, -25.31401921878175898, 5.197788989978544549 ) ) ;
#83792=CARTESIAN_POINT ( 'NONE',  ( 8.471766090126642723, -20.80389698432254519, -1.500000000000002220 ) ) ;
#83793=B_SPLINE_SURFACE_WITH_KNOTS ( 'NONE', 3, 3, ( 
 ( #30184, #9219, #30690, #44938 ),
 ( #92087, #61661, #53548, #32560 ),
 ( #84478, #14958, #92579, #40182 ),
 ( #45932, #63538, #69255, #17338 ),
 ( #94463, #71134, #75860, #6363 ),
 ( #24944, #55921, #86842, #37320 ),
 ( #79231, #52539, #9730, #33071 ) ),
 .UNSPECIFIED., .F., .F., .F.,
 ( 4, 3, 4 ),
 ( 4, 4 ),
 ( 0.0004766839783834332330, 0.1029713700210900112, 0.2054660560637965871 ),
 ( 0.9597381382339776890, 0.9611936842035376793 ),
 .UNSPECIFIED. ) ;
#83794=CARTESIAN_POINT ( 'NONE',  ( -108.8764474181941040, -25.31476271379807841, 5.144092056987718209 ) ) ;
#83795=EDGE_LOOP ( 'NONE', ( #70711, #61229, #85153, #12396 ) ) ;
#83796=B_SPLINE_CURVE_WITH_KNOTS ( 'NONE', 3,
 ( #9305, #64640, #39758, #70718 ),
 .UNSPECIFIED., .F., .F.,
 ( 4, 4 ),
 ( 0.6102216688345595275, 0.6192281001066749502 ),
 .UNSPECIFIED. ) ;
#83797=DIRECTION ( 'NONE',  ( 1.000000000000000000, 3.773278334444167608E-23, 8.201307833595939069E-29 ) ) ;
#83798=CARTESIAN_POINT ( 'NONE',  ( 5.347671334029483248, -18.86178030415664963, 11.49999999999999645 ) ) ;
#83799=CARTESIAN_POINT ( 'NONE',  ( -68.62287095715004170, -24.50216790748098816, 0.6166512839513629274 ) ) ;
#83802=ORIENTED_EDGE ( 'NONE', *, *, #82579, .T. ) ;
#83804=CARTESIAN_POINT ( 'NONE',  ( -70.18625720459044715, -25.30468007125771379, 4.853999493951613786 ) ) ;
#83805=CARTESIAN_POINT ( 'NONE',  ( -36.52287095715008292, -23.72773821059535848, 11.05748984161097326 ) ) ;
#83806=CARTESIAN_POINT ( 'NONE',  ( -100.6373084487711225, -25.25095777383906892, 5.200261160962469376 ) ) ;
#83808=CARTESIAN_POINT ( 'NONE',  ( -122.5562042904834072, -23.47593901973091235, -1.443836447538997536 ) ) ;
#83809=CARTESIAN_POINT ( 'NONE',  ( -9.502044936771568473, -17.27029980899984452, -1.500000000000002220 ) ) ;
#83813=CARTESIAN_POINT ( 'NONE',  ( -118.5228709571500758, -24.65952944569305316, 1.056160979905705899 ) ) ;
#83814=B_SPLINE_CURVE_WITH_KNOTS ( 'NONE', 3,
 ( #94512, #165, #54962, #63081 ),
 .UNSPECIFIED., .F., .F.,
 ( 4, 4 ),
 ( 0.3600430223869087176, 0.3690494536590239738 ),
 .UNSPECIFIED. ) ;
#83815=EDGE_CURVE ( 'NONE', #90352, #26998, #52745, .T. ) ;
#83818=ORIENTED_EDGE ( 'NONE', *, *, #39671, .F. ) ;
#83820=CARTESIAN_POINT ( 'NONE',  ( -67.62287095715012697, -24.34917612406838572, 0.1852690917426630390 ) ) ;
#83821=CARTESIAN_POINT ( 'NONE',  ( -98.89994392110364174, -25.03144904247453795, 6.299691620028943895 ) ) ;
#83822=CARTESIAN_POINT ( 'NONE',  ( -49.55620429048337883, -24.64965694238574301, 8.947790433994201820 ) ) ;
#83823=AXIS2_PLACEMENT_3D ( 'NONE', #14645, #93264, #7537 ) ;
#83824=CARTESIAN_POINT ( 'NONE',  ( -69.88050735872322150, -25.24515064012728160, 5.413835170906579286 ) ) ;
#83825=CARTESIAN_POINT ( 'NONE',  ( -91.52287095715006160, -23.47596703998600631, 11.44779298504228393 ) ) ;
#83826=CARTESIAN_POINT ( 'NONE',  ( -8.876215969300202957, 17.89991547088461488, 11.49999999999998934 ) ) ;
#83829=CARTESIAN_POINT ( 'NONE',  ( -45.65167645653958317, -24.15602025860896163, 10.28564288303535434 ) ) ;
#83832=EDGE_CURVE ( 'NONE', #38212, #46658, #94277, .T. ) ;
#83833=CARTESIAN_POINT ( 'NONE',  ( -66.52287095715006160, -23.48783264082476663, -1.443836473390092134 ) ) ;
#83834=CARTESIAN_POINT ( 'NONE',  ( -80.49976769349017047, -24.63419186844610920, 9.035850630976922204 ) ) ;
#83836=CARTESIAN_POINT ( 'NONE',  ( -81.54105079080106577, -24.65952944569304961, 1.056160979905703901 ) ) ;
#83838=CARTESIAN_POINT ( 'NONE',  ( -51.33061876479827390, -25.31574422701022087, 4.756068479901139234 ) ) ;
#83839=DIRECTION ( 'NONE',  ( -1.000000000000000000, -3.773278334444166432E-23, -8.201307841325785021E-29 ) ) ;
#83842=CARTESIAN_POINT ( 'NONE',  ( -5.286950244708777724, -19.55949958832428948, 11.49999999999998934 ) ) ;
#83846=CARTESIAN_POINT ( 'NONE',  ( -99.62287095715005592, -23.72747288104441665, -1.053458166803661111 ) ) ;
#83849=B_SPLINE_CURVE_WITH_KNOTS ( 'NONE', 3,
 ( #95276, #96276, #73445, #58227 ),
 .UNSPECIFIED., .F., .F.,
 ( 4, 4 ),
 ( 0.000000000000000000, 0.0001000000000000028644 ),
 .UNSPECIFIED. ) ;
#83850=CARTESIAN_POINT ( 'NONE',  ( -63.62287095715002749, -24.33832256526968862, 0.1851278514119841789 ) ) ;
#83851=CARTESIAN_POINT ( 'NONE',  ( 5.780499401231428358, -19.25771307485560158, -1.500000000000002220 ) ) ;
#83852=CARTESIAN_POINT ( 'NONE',  ( -12.45680796028966597, 17.00782699154285638, 11.49999999999999645 ) ) ;
#83853=AXIS2_PLACEMENT_3D ( 'NONE', #65509, #19292, #50263 ) ;
#83854=CARTESIAN_POINT ( 'NONE',  ( -100.4426124108961176, -29.50249842297920466, 7.101626040072651413 ) ) ;
#83855=CARTESIAN_POINT ( 'NONE',  ( -22.12685673520133989, -0.1325007643398395663, -1.500000000000002220 ) ) ;
#83856=CARTESIAN_POINT ( 'NONE',  ( 20.53815866822273861, -0.6333348845813139283, -1.500000000000002220 ) ) ;
#83857=CARTESIAN_POINT ( 'NONE',  ( -35.58953762381672448, -24.99132157543083821, 2.256160258750496084 ) ) ;
#83861=EDGE_LOOP ( 'NONE', ( #70529, #99221, #11528, #9384 ) ) ;
#83865=ORIENTED_EDGE ( 'NONE', *, *, #97893, .T. ) ;
#83866=CARTESIAN_POINT ( 'NONE',  ( -65.52287095715006160, -23.48783264082476308, -1.443836473390092578 ) ) ;
#83869=CARTESIAN_POINT ( 'NONE',  ( 18.09409571311175569, -9.955296453752364272, -1.500000000000002220 ) ) ;
#83870=CARTESIAN_POINT ( 'NONE',  ( -19.98381242416700587, 8.274006965216138099, 11.49999999999999645 ) ) ;
#83872=DIRECTION ( 'NONE',  ( -3.773278334453079030E-23, 0.9999999999976377785, 2.173523156925979128E-06 ) ) ;
#83874=CARTESIAN_POINT ( 'NONE',  ( 21.65046080595755740, -5.567969076317650590, -1.500000000000002220 ) ) ;
#83876=CARTESIAN_POINT ( 'NONE',  ( -62.52287095715004739, -24.34917612406836795, 0.1852690917426548511 ) ) ;
#83878=ORIENTED_EDGE ( 'NONE', *, *, #24626, .F. ) ;
#83881=CARTESIAN_POINT ( 'NONE',  ( 8.468106961216914641, 19.09613275528424836, 11.49999999999998934 ) ) ;
#83882=ORIENTED_EDGE ( 'NONE', *, *, #22255, .F. ) ;
#83883=CARTESIAN_POINT ( 'NONE',  ( -98.62287095715005592, -23.94994826722515668, -0.6494450866351687557 ) ) ;
#83884=EDGE_LOOP ( 'NONE', ( #25985, #99210, #94762, #18418 ) ) ;
#83887=CARTESIAN_POINT ( 'NONE',  ( -109.5537012376542236, -24.15620529776628445, 10.23563542870660115 ) ) ;
#83888=CARTESIAN_POINT ( 'NONE',  ( -12.37649675270136918, 17.12833386298736471, -1.500000000000002220 ) ) ;
#83889=VERTEX_POINT ( 'NONE', #88181 ) ;
#83890=CARTESIAN_POINT ( 'NONE',  ( -117.5912916562027419, -23.96119346886881019, -0.6495511937831995875 ) ) ;
#83891=CARTESIAN_POINT ( 'NONE',  ( -100.4426124108961176, -25.26221318251349146, 7.101635256430813392 ) ) ;
#83892=EDGE_CURVE ( 'NONE', #27379, #11225, #35857, .T. ) ;
#83893=CARTESIAN_POINT ( 'NONE',  ( -8.334044162642690878, 20.12857247364870616, -1.500000000000002220 ) ) ;
#83894=LINE ( 'NONE', #43851, #62704 ) ;
#83897=CARTESIAN_POINT ( 'NONE',  ( -36.62287095715006302, -23.72747288104469732, -1.053458166803227902 ) ) ;
#83898=B_SPLINE_CURVE_WITH_KNOTS ( 'NONE', 3,
 ( #60399, #15193, #84201, #93310 ),
 .UNSPECIFIED., .F., .F.,
 ( 4, 4 ),
 ( 0.000000000000000000, 0.0001000000000000028644 ),
 .UNSPECIFIED. ) ;
#83900=CARTESIAN_POINT ( 'NONE',  ( -18.42844947050907578, 11.51566461966115540, -1.500000000000002220 ) ) ;
#83902=CARTESIAN_POINT ( 'NONE',  ( 13.91197278145025074, 17.48688927191260234, 11.49999999999999645 ) ) ;
#83904=CARTESIAN_POINT ( 'NONE',  ( -33.52287095715004739, -23.73907113217656573, -1.053371485781500860 ) ) ;
#83905=CARTESIAN_POINT ( 'NONE',  ( -85.49558110888244755, -25.00182538069147142, 7.747789668545045139 ) ) ;
#83906=CARTESIAN_POINT ( 'NONE',  ( -68.62287095715005592, -24.65952944569304606, 1.056160979905698794 ) ) ;
#83907=VERTEX_POINT ( 'NONE', #75422 ) ;
#83908=EDGE_CURVE ( 'NONE', #7838, #67776, #62451, .T. ) ;
#83910=ORIENTED_EDGE ( 'NONE', *, *, #18486, .F. ) ;
#83913=CARTESIAN_POINT ( 'NONE',  ( 20.79131504077403747, 4.132458064796619368, 11.49999999999998934 ) ) ;
#83914=CARTESIAN_POINT ( 'NONE',  ( -127.6228709571500559, -23.47593901973091235, -1.443836447538995760 ) ) ;
#83915=CARTESIAN_POINT ( 'NONE',  ( -79.70355613134685768, -25.03138256630352387, 7.365681602826161800 ) ) ;
#83916=CARTESIAN_POINT ( 'NONE',  ( -41.52287095715006870, -23.47593901973090169, -1.443836447538997092 ) ) ;
#83917=B_SPLINE_CURVE_WITH_KNOTS ( 'NONE', 3,
 ( #88264, #18737, #42602, #89760, #74037, #26859 ),
 .UNSPECIFIED., .F., .F.,
 ( 4, 2, 4 ),
 ( 0.000000000000000000, 0.001380764517854764532, 0.002761529035709529064 ),
 .UNSPECIFIED. ) ;
#83919=CARTESIAN_POINT ( 'NONE',  ( -84.62287095715005592, -29.50250243563736774, 8.947779886222141599 ) ) ;
#83920=CARTESIAN_POINT ( 'NONE',  ( -45.62316515138000028, -23.48783264082476663, -1.443836473390103237 ) ) ;
#83921=ORIENTED_EDGE ( 'NONE', *, *, #29037, .T. ) ;
#83922=CARTESIAN_POINT ( 'NONE',  ( -7.499459838998954631, -17.95702976299720532, 11.49999999999999645 ) ) ;
#83923=CARTESIAN_POINT ( 'NONE',  ( -69.52287095715006160, -24.64898659630367916, 1.056161002820824368 ) ) ;
#83924=EDGE_LOOP ( 'NONE', ( #64220, #58008, #22982, #80521 ) ) ;
#83929=DIRECTION ( 'NONE',  ( -3.773278334453079618E-23, 0.9999999999976377785, 2.173523156925979975E-06 ) ) ;
#83930=CARTESIAN_POINT ( 'NONE',  ( 14.10018531369908423, 13.67006465538575277, 11.49999999999998934 ) ) ;
#83932=B_SPLINE_SURFACE_WITH_KNOTS ( 'NONE', 3, 3, ( 
 ( #98502, #13761, #98998, #29492 ),
 ( #37114, #91890, #99497, #60967 ),
 ( #74674, #53352, #91392, #90902 ),
 ( #75172, #13268, #14262, #44739 ),
 ( #69063, #52845, #36123, #60474 ),
 ( #92391, #68569, #67584, #5170 ),
 ( #67094, #37614, #76654, #7157 ) ),
 .UNSPECIFIED., .F., .F., .F.,
 ( 4, 3, 4 ),
 ( 4, 4 ),
 ( 0.7945040050992242531, 0.8970133687736501216, 0.9995227324480759901 ),
 ( 0.4596107907157971906, 0.4608357021111512686 ),
 .UNSPECIFIED. ) ;
#83935=CARTESIAN_POINT ( 'NONE',  ( -17.67581969798968444, -12.36387604476075097, -1.500000000000002220 ) ) ;
#83936=CARTESIAN_POINT ( 'NONE',  ( -43.62287095715004881, -23.47593901973091235, -1.443836447539011525 ) ) ;
#83938=LINE ( 'NONE', #69723, #41022 ) ;
#83939=CARTESIAN_POINT ( 'NONE',  ( -100.2462005486704442, -25.18439338411695161, 3.306208445075104585 ) ) ;
#83940=CARTESIAN_POINT ( 'NONE',  ( -23.02147672596084149, 0.6323230698326208765, -1.500000000000002220 ) ) ;
#83942=CARTESIAN_POINT ( 'NONE',  ( -56.22287095715007155, -23.47596703998600276, 11.44779298504227860 ) ) ;
#83943=CARTESIAN_POINT ( 'NONE',  ( -96.52287095715006160, -23.47596703998600631, 11.44779298504228215 ) ) ;
#83944=CARTESIAN_POINT ( 'NONE',  ( -14.78635263257777233, 13.65558988533819473, 11.49999999999999645 ) ) ;
#83945=CARTESIAN_POINT ( 'NONE',  ( -109.7637679387061809, -25.10927417198714906, 2.928686727655255062 ) ) ;
#83947=CARTESIAN_POINT ( 'NONE',  ( -46.52287095715005449, -24.51283580621365843, 0.6167428607019604936 ) ) ;
#83949=CARTESIAN_POINT ( 'NONE',  ( -110.7296117302316532, -25.29779169913011572, 3.360882835270145641 ) ) ;
#83950=CARTESIAN_POINT ( 'NONE',  ( 12.81631318294326505, -15.22695477405695996, 11.49999999999998934 ) ) ;
#83952=CARTESIAN_POINT ( 'NONE',  ( -14.06767371131996214, 13.90018863433869889, -1.500000000000002220 ) ) ;
#83954=CARTESIAN_POINT ( 'NONE',  ( -126.6234820425866872, -24.66019654487200796, 8.947790411086103290 ) ) ;
#83957=B_SPLINE_CURVE_WITH_KNOTS ( 'NONE', 3,
 ( #28023, #44250, #96528, #59471, #28510, #35142 ),
 .UNSPECIFIED., .F., .F.,
 ( 4, 2, 4 ),
 ( 6.384118695446109541E-06, 0.001386860460836795116, 0.002767336802978144061 ),
 .UNSPECIFIED. ) ;
#83959=CARTESIAN_POINT ( 'NONE',  ( -14.21563987850626276, 15.01860006206015008, 11.49999999999999645 ) ) ;
#83960=CARTESIAN_POINT ( 'NONE',  ( -58.52287095715007581, -24.50216790748205398, 0.6166512839542500624 ) ) ;
#83961=EDGE_CURVE ( 'NONE', #38812, #29553, #90168, .T. ) ;
#83962=CARTESIAN_POINT ( 'NONE',  ( -79.52287095715006160, -23.47596703998600631, 11.44779298504228571 ) ) ;
#83963=CARTESIAN_POINT ( 'NONE',  ( 1.118074629359579797, -22.68859683979520980, 11.49999999999999645 ) ) ;
#83964=EDGE_LOOP ( 'NONE', ( #33934, #92732, #82903, #67876 ) ) ;
#83966=CARTESIAN_POINT ( 'NONE',  ( -74.62287095715004170, -24.66019654487199375, 8.947790411086129936 ) ) ;
#83967=AXIS2_PLACEMENT_3D ( 'NONE', #58403, #72625, #10719 ) ;
#83968=CARTESIAN_POINT ( 'NONE',  ( -18.82377384687745447, 7.257840063761761051, 11.49999999999998934 ) ) ;
#83969=CARTESIAN_POINT ( 'NONE',  ( -63.56611337692685737, -23.48783264082476308, -1.443836473390093245 ) ) ;
#83970=CARTESIAN_POINT ( 'NONE',  ( -54.62287095715005592, -29.50250243563736774, 8.947779886222146928 ) ) ;
#83971=ORIENTED_EDGE ( 'NONE', *, *, #92093, .F. ) ;
#83972=EDGE_LOOP ( 'NONE', ( #37817, #48058, #72924, #13021 ) ) ;
#83974=CARTESIAN_POINT ( 'NONE',  ( 21.34038654641452482, 8.310931564070170197, 11.49999999999998934 ) ) ;
#83975=CARTESIAN_POINT ( 'NONE',  ( -50.83488094104556154, -25.27420580424551133, 3.373740132572621953 ) ) ;
#83976=CARTESIAN_POINT ( 'NONE',  ( 7.043455336710909620, -20.48365140995157674, -1.500000000000002220 ) ) ;
#83978=DIRECTION ( 'NONE',  ( 0.000000000000000000, 2.173523156925980399E-06, -0.9999999999976378895 ) ) ;
#83980=CARTESIAN_POINT ( 'NONE',  ( -17.10473743203234775, -12.04273770408705246, 11.49999999999999645 ) ) ;
#83981=VERTEX_POINT ( 'NONE', #20148 ) ;
#83982=FACE_OUTER_BOUND ( 'NONE', #73919, .T. ) ;
#83983=CARTESIAN_POINT ( 'NONE',  ( -15.01370250125036421, 16.05796621403891677, -1.500000000000002220 ) ) ;
#83984=CARTESIAN_POINT ( 'NONE',  ( -105.6347233272999944, -23.85049219812686871, 10.88485053497526955 ) ) ;
#83985=CARTESIAN_POINT ( 'NONE',  ( -41.82812249501711932, -25.10925988035710077, 3.843615596726369432 ) ) ;
#83987=B_SPLINE_CURVE_WITH_KNOTS ( 'NONE', 3,
 ( #43337, #27611, #74276, #4767 ),
 .UNSPECIFIED., .F., .F.,
 ( 4, 4 ),
 ( 0.000000000000000000, 0.0001000000000000028644 ),
 .UNSPECIFIED. ) ;
#83989=FACE_OUTER_BOUND ( 'NONE', #77400, .T. ) ;
#83990=VERTEX_POINT ( 'NONE', #35881 ) ;
#83991=PLANE ( 'NONE',  #98732 ) ;
#83994=CARTESIAN_POINT ( 'NONE',  ( -59.52287095715009002, -23.47593901973090524, -1.443836447538997092 ) ) ;
#83996=CARTESIAN_POINT ( 'NONE',  ( -57.59300200441531103, -24.15543982623907127, -0.2315651400026663420 ) ) ;
#83997=CARTESIAN_POINT ( 'NONE',  ( 0.3735783541106268979, -20.45636175344465713, -1.500000000000002220 ) ) ;
#83998=B_SPLINE_CURVE_WITH_KNOTS ( 'NONE', 3,
 ( #76177, #68585, #77674, #60980, #83799, #14279 ),
 .UNSPECIFIED., .F., .F.,
 ( 4, 2, 4 ),
 ( 0.000000000000000000, 0.001380764517853250118, 0.002761529035706500237 ),
 .UNSPECIFIED. ) ;
#83999=ORIENTED_EDGE ( 'NONE', *, *, #75926, .F. ) ;
#84000=CARTESIAN_POINT ( 'NONE',  ( -93.58953762381672448, -24.64965694238575011, 8.947790433994196491 ) ) ;
#84002=CARTESIAN_POINT ( 'NONE',  ( -98.62287095715004170, -24.65952944569304606, 1.056160979905700792 ) ) ;
#84003=CARTESIAN_POINT ( 'NONE',  ( -25.77888769185907947, -24.80838911334880592, 6.758736707713437930 ) ) ;
#84006=CARTESIAN_POINT ( 'NONE',  ( -64.62287095715005592, -23.48786465467241413, 11.44779295918254824 ) ) ;
#84007=CARTESIAN_POINT ( 'NONE',  ( 13.57807927624399902, 15.74560944506941951, 11.49999999999998934 ) ) ;
#84010=VERTEX_POINT ( 'NONE', #98260 ) ;
#84011=B_SPLINE_SURFACE_WITH_KNOTS ( 'NONE', 3, 3, ( 
 ( #90136, #51580, #81031, #73422 ),
 ( #3920, #65824, #80672, #71573 ),
 ( #42628, #58352, #3065, #19263 ),
 ( #10666, #17780, #56361, #88798 ),
 ( #89288, #73566, #41628, #72570 ),
 ( #95399, #34005, #65980, #87279 ),
 ( #19754, #50730, #49248, #64981 ) ),
 .UNSPECIFIED., .F., .F., .F.,
 ( 4, 3, 4 ),
 ( 4, 4 ),
 ( 0.0004766839783821298594, 0.1029713700210898308, 0.2054660560637975308 ),
 ( 0.2895676583132508197, 0.2907139888547707884 ),
 .UNSPECIFIED. ) ;
#84012=CARTESIAN_POINT ( 'NONE',  ( -50.56357725185049645, -25.12217861855133094, 7.098062342091831844 ) ) ;
#84015=LINE ( 'NONE', #14503, #5752 ) ;
#84016=CARTESIAN_POINT ( 'NONE',  ( -55.62287095715004170, -23.47596703998600631, 11.44779298504227505 ) ) ;
#84017=EDGE_CURVE ( 'NONE', #32236, #65202, #38159, .T. ) ;
#84019=CARTESIAN_POINT ( 'NONE',  ( -100.4498239493576506, -25.03152449170482186, 7.563174219377576613 ) ) ;
#84020=CARTESIAN_POINT ( 'NONE',  ( -92.59142756244220607, -24.15620529776628445, 10.23563542870660292 ) ) ;
#84021=PLANE ( 'NONE',  #52987 ) ;
#84022=CARTESIAN_POINT ( 'NONE',  ( 21.13975321936677787, -6.629177502137091338, 11.49999999999999645 ) ) ;
#84023=VERTEX_POINT ( 'NONE', #51112 ) ;
#84026=CARTESIAN_POINT ( 'NONE',  ( -22.43363504178351775, 2.973318333978472339, 11.49999999999998934 ) ) ;
#84028=EDGE_CURVE ( 'NONE', #83477, #52082, #23603, .T. ) ;
#84029=CARTESIAN_POINT ( 'NONE',  ( -80.52287095715006160, -24.99156044556202616, 7.747789690856173195 ) ) ;
#84030=EDGE_LOOP ( 'NONE', ( #69670, #84632, #56690, #98458 ) ) ;
#84031=EDGE_CURVE ( 'NONE', #61594, #91753, #21140, .T. ) ;
#84032=ORIENTED_EDGE ( 'NONE', *, *, #88185, .F. ) ;
#84033=B_SPLINE_CURVE_WITH_KNOTS ( 'NONE', 3,
 ( #31708, #14975, #255, #38314 ),
 .UNSPECIFIED., .F., .F.,
 ( 4, 4 ),
 ( 3.706435412536978550E-09, 0.0004668278787522539683 ),
 .UNSPECIFIED. ) ;
#84034=EDGE_CURVE ( 'NONE', #9262, #85354, #606, .T. ) ;
#84036=CARTESIAN_POINT ( 'NONE',  ( 6.436487395234643749, 19.08016507665710648, -1.500000000000002220 ) ) ;
#84037=B_SPLINE_CURVE_WITH_KNOTS ( 'NONE', 3,
 ( #7655, #84272, #36605, #85270, #46727, #45230, #76153, #7148, #92383, #91883, #6652, #75652 ),
 .UNSPECIFIED., .F., .F.,
 ( 4, 2, 2, 2, 2, 4 ),
 ( 0.000000000000000000, 0.0001590846665151804601, 0.0003181693330303609203, 0.0006363386660606980966, 0.0009545079990910353271, 0.001272677332121372558 ),
 .UNSPECIFIED. ) ;
#84042=CARTESIAN_POINT ( 'NONE',  ( 3.752539591237177508, -22.04708138622333635, -1.500000000000002220 ) ) ;
#84044=ORIENTED_EDGE ( 'NONE', *, *, #43839, .T. ) ;
#84045=ORIENTED_EDGE ( 'NONE', *, *, #45717, .F. ) ;
#84046=LINE ( 'NONE', #39372, #72461 ) ;
#84047=CARTESIAN_POINT ( 'NONE',  ( -116.6228709571500559, -24.64965695001469115, 8.947790433994175174 ) ) ;
#84049=CARTESIAN_POINT ( 'NONE',  ( -96.62287095714999907, -24.51387760970724372, 9.387446482453412955 ) ) ;
#84051=CARTESIAN_POINT ( 'NONE',  ( 2.510080532074158377, -19.39449211012750496, -1.500000000000002220 ) ) ;
#84052=LINE ( 'NONE', #14534, #10181 ) ;
#84053=CARTESIAN_POINT ( 'NONE',  ( -17.67684169981329845, 12.20363403927300183, -1.500000000000002220 ) ) ;
#84054=CARTESIAN_POINT ( 'NONE',  ( -25.53098197642538736, -24.92775386671257465, 4.942811681260474543 ) ) ;
#84055=CARTESIAN_POINT ( 'NONE',  ( -120.5228709571500474, -24.63287334234178516, 0.9662140553045437397 ) ) ;
#84057=CARTESIAN_POINT ( 'NONE',  ( -15.36296916364455711, -16.94538937337987150, -1.500000000000002220 ) ) ;
#84059=DIRECTION ( 'NONE',  ( -1.000000000000000000, -3.773278334444166432E-23, -8.201307841325785021E-29 ) ) ;
#84061=CARTESIAN_POINT ( 'NONE',  ( -8.813339738934139689, -17.91118242276673911, 11.49999999999999645 ) ) ;
#84062=DIRECTION ( 'NONE',  ( 1.000000000000000000, 3.773278334444166432E-23, 8.201307841325785021E-29 ) ) ;
#84063=CARTESIAN_POINT ( 'NONE',  ( -74.55900445870243232, -23.73791477778911840, 11.05961554403170588 ) ) ;
#84064=CARTESIAN_POINT ( 'NONE',  ( -75.52287095715007581, -23.47593901973090169, -1.443836447538996870 ) ) ;
#84065=VERTEX_POINT ( 'NONE', #4934 ) ;
#84066=DIRECTION ( 'NONE',  ( 0.000000000000000000, -2.173523156925979552E-06, 0.9999999999976378895 ) ) ;
#84069=CARTESIAN_POINT ( 'NONE',  ( -8.443908442993951269, 20.02826104456839218, -1.500000000000002220 ) ) ;
#84070=DIRECTION ( 'NONE',  ( 3.773278334444166432E-23, -1.000000000000000000, 0.000000000000000000 ) ) ;
#84071=CARTESIAN_POINT ( 'NONE',  ( -19.07250549579359244, -4.594354733287289605, -1.500000000000002220 ) ) ;
#84072=LINE ( 'NONE', #51640, #24775 ) ;
#84073=VERTEX_POINT ( 'NONE', #89175 ) ;
#84074=DIRECTION ( 'NONE',  ( 0.06471892502635213928, -0.8378373432121152264, 0.5420701495772458633 ) ) ;
#84075=CARTESIAN_POINT ( 'NONE',  ( -47.52287095715010423, -24.33927499327855770, 9.819080762295813614 ) ) ;
#84076=CARTESIAN_POINT ( 'NONE',  ( -11.60840874443078263, -16.91462557209307960, 11.49999999999999645 ) ) ;
#84082=EDGE_CURVE ( 'NONE', #94218, #76361, #58235, .T. ) ;
#84091=AXIS2_PLACEMENT_3D ( 'NONE', #9830, #2736, #10838 ) ;
#84092=CARTESIAN_POINT ( 'NONE',  ( -8.701767255460435280, 21.38705905713849020, 11.49999999999999645 ) ) ;
#84093=CARTESIAN_POINT ( 'NONE',  ( -2.657479817400386413, -22.66247145590962120, -1.500000000000002220 ) ) ;
#84094=CARTESIAN_POINT ( 'NONE',  ( -110.5169826798708925, -24.15602025860899360, 10.28564288303533480 ) ) ;
#84095=CARTESIAN_POINT ( 'NONE',  ( -75.52287095715011844, -24.62285846331433703, 9.038163153548364193 ) ) ;
#84096=CARTESIAN_POINT ( 'NONE',  ( -119.5228709571500758, -24.64898659630368627, 1.056161002820833028 ) ) ;
#84098=CARTESIAN_POINT ( 'NONE',  ( -119.5228709571500758, -29.50250243563736774, 8.947779886222134493 ) ) ;
#84100=CARTESIAN_POINT ( 'NONE',  ( 12.66425630052701479, 17.85959152241435177, 11.49999999999998934 ) ) ;
#84103=B_SPLINE_CURVE_WITH_KNOTS ( 'NONE', 3,
 ( #52680, #7494, #90741, #100320 ),
 .UNSPECIFIED., .F., .F.,
 ( 4, 4 ),
 ( 0.000000000000000000, 9.999999999998897304E-05 ),
 .UNSPECIFIED. ) ;
#84104=LINE ( 'NONE', #46552, #15513 ) ;
#84105=PLANE ( 'NONE',  #40592 ) ;
#84106=CARTESIAN_POINT ( 'NONE',  ( -78.50135358901988525, -24.51314013834315375, 0.6176544820404143987 ) ) ;
#84107=FACE_OUTER_BOUND ( 'NONE', #69409, .T. ) ;
#84108=FACE_OUTER_BOUND ( 'NONE', #43940, .T. ) ;
#84109=EDGE_LOOP ( 'NONE', ( #44883, #94479, #39820, #50528 ) ) ;
#84111=CARTESIAN_POINT ( 'NONE',  ( 2.691128592823461840, 20.25793168094256202, 11.49999999999998934 ) ) ;
#84113=ORIENTED_EDGE ( 'NONE', *, *, #81874, .F. ) ;
#84115=ORIENTED_EDGE ( 'NONE', *, *, #73948, .F. ) ;
#84116=CARTESIAN_POINT ( 'NONE',  ( -8.497478458550677516, -21.44862750780143656, 11.49999999999998934 ) ) ;
#84118=CARTESIAN_POINT ( 'NONE',  ( -16.64171244834553676, 11.49637152377623828, -1.500000000000002220 ) ) ;
#84119=EDGE_LOOP ( 'NONE', ( #70099, #5659, #84727, #1785 ) ) ;
#84120=CARTESIAN_POINT ( 'NONE',  ( -28.20266704546411773, -25.12201335372101596, 4.938174481708933250 ) ) ;
#84121=CARTESIAN_POINT ( 'NONE',  ( -37.52287095715006870, -23.47593901973090524, -1.443836447538997314 ) ) ;
#84122=CARTESIAN_POINT ( 'NONE',  ( -94.22287095715005023, -23.47596703998600631, 11.44779298504227860 ) ) ;
#84123=CARTESIAN_POINT ( 'NONE',  ( -99.59111425744799817, -24.15620529776628445, 10.23563542870660115 ) ) ;
#84124=CARTESIAN_POINT ( 'NONE',  ( 14.05358622956002357, 16.19628355576825385, 11.49999999999999645 ) ) ;
#84126=CARTESIAN_POINT ( 'NONE',  ( -128.6228709571500417, -24.50216790748099882, 0.6166512839513794697 ) ) ;
#84127=CARTESIAN_POINT ( 'NONE',  ( -61.57930063205219540, -24.66019654487199375, 8.947790411086119278 ) ) ;
#84128=ORIENTED_EDGE ( 'NONE', *, *, #18950, .F. ) ;
#84129=CARTESIAN_POINT ( 'NONE',  ( -19.40401905104624802, 7.283777608679691262, -1.500000000000002220 ) ) ;
#84133=CARTESIAN_POINT ( 'NONE',  ( -65.52287095715006160, -23.48783264082476308, -1.443836473390092578 ) ) ;
#84134=ORIENTED_EDGE ( 'NONE', *, *, #16248, .F. ) ;
#84136=CARTESIAN_POINT ( 'NONE',  ( -35.52287095715006870, -23.47596703998600631, 11.44779298504229281 ) ) ;
#84137=CARTESIAN_POINT ( 'NONE',  ( -18.27885182143903720, 12.20952002138517045, 11.49999999999999645 ) ) ;
#84138=CARTESIAN_POINT ( 'NONE',  ( -89.58353286622173073, -24.66019654487199730, 8.947790411086115725 ) ) ;
#84139=CARTESIAN_POINT ( 'NONE',  ( 9.831018646898828095, -20.30805102056165623, -1.500000000000002220 ) ) ;
#84140=CARTESIAN_POINT ( 'NONE',  ( -7.180602670292889123, -19.69607742855361465, 11.49999999999998934 ) ) ;
#84141=DIRECTION ( 'NONE',  ( -3.773278334444166432E-23, 1.000000000000000000, 0.000000000000000000 ) ) ;
#84143=CARTESIAN_POINT ( 'NONE',  ( -30.64752034897746924, -23.47593901973090169, -1.443836447538997758 ) ) ;
#84147=ORIENTED_EDGE ( 'NONE', *, *, #70736, .F. ) ;
#84148=EDGE_CURVE ( 'NONE', #77901, #13356, #84046, .T. ) ;
#84149=CARTESIAN_POINT ( 'NONE',  ( -66.60300269009690055, -23.73766607897669800, -1.055555164236460897 ) ) ;
#84150=CARTESIAN_POINT ( 'NONE',  ( 19.30674495121141376, 9.566621930910674365, -1.500000000000002220 ) ) ;
#84153=CARTESIAN_POINT ( 'NONE',  ( -16.61111445048470614, -13.04167290785011701, 11.49999999999998934 ) ) ;
#84154=CARTESIAN_POINT ( 'NONE',  ( -67.62287095715005592, -23.47593901973091235, -1.443836447539006196 ) ) ;
#84155=LINE ( 'NONE', #22243, #1122 ) ;
#84156=CARTESIAN_POINT ( 'NONE',  ( -83.51756172583068860, -23.73791477778911840, 11.05961554403170588 ) ) ;
#84159=CARTESIAN_POINT ( 'NONE',  ( 9.107982344273736430, -20.20341329189913537, -1.500000000000002220 ) ) ;
#84160=CARTESIAN_POINT ( 'NONE',  ( -71.60196529453079961, -23.73766607897669800, -1.055555164236456012 ) ) ;
#84162=ORIENTED_EDGE ( 'NONE', *, *, #67890, .T. ) ;
#84165=CARTESIAN_POINT ( 'NONE',  ( -43.52287095715006160, -29.50250243563736774, 8.947779886222148704 ) ) ;
#84167=CARTESIAN_POINT ( 'NONE',  ( -97.52287095715010423, -23.95044443724993144, 10.65354141964649415 ) ) ;
#84169=CARTESIAN_POINT ( 'NONE',  ( -19.16120753946698585, -3.443109951913609024, -1.500000000000002220 ) ) ;
#84170=VECTOR ( 'NONE', #28326, 1000.000000000000227 ) ;
#84171=CARTESIAN_POINT ( 'NONE',  ( -10.59417575825165159, 18.57464501519095279, 11.49999999999998934 ) ) ;
#84173=CARTESIAN_POINT ( 'NONE',  ( -37.52287095715006870, -29.50248528299804818, 1.056150453629031594 ) ) ;
#84174=CARTESIAN_POINT ( 'NONE',  ( -122.6228709571500417, -24.64965695001469115, 8.947790433994175174 ) ) ;
#84175=CARTESIAN_POINT ( 'NONE',  ( -100.4326965455115186, -25.18440011175262683, 3.293943117858023406 ) ) ;
#84176=CARTESIAN_POINT ( 'NONE',  ( 13.52301212282245935, 18.22803923376396540, -1.500000000000002220 ) ) ;
#84177=VECTOR ( 'NONE', #39345, 1000.000000000000114 ) ;
#84179=CARTESIAN_POINT ( 'NONE',  ( -31.62287095715005236, -23.47593901973091235, -1.443836447539013301 ) ) ;
#84180=CARTESIAN_POINT ( 'NONE',  ( -57.62287095715002039, -24.51387760970723662, 9.387446482453421837 ) ) ;
#84181=CARTESIAN_POINT ( 'NONE',  ( -15.05033210666397103, 12.90603908704162173, 11.49999999999999645 ) ) ;
#84182=CARTESIAN_POINT ( 'NONE',  ( -35.52287095715006870, -25.00158670708909270, 2.256160236439166411 ) ) ;
#84183=ORIENTED_EDGE ( 'NONE', *, *, #5921, .T. ) ;
#84185=DIRECTION ( 'NONE',  ( 0.000000000000000000, -2.173523156925980399E-06, 0.9999999999976378895 ) ) ;
#84186=CARTESIAN_POINT ( 'NONE',  ( -3.891998276399621481, 21.28400606017829233, -1.500000000000002220 ) ) ;
#84187=CARTESIAN_POINT ( 'NONE',  ( -49.27110903475092130, -25.10935255461681237, 3.423268907010238671 ) ) ;
#84188=CARTESIAN_POINT ( 'NONE',  ( 16.99290379607386114, -9.356058476803225332, -1.500000000000002220 ) ) ;
#84190=CARTESIAN_POINT ( 'NONE',  ( -35.62287095715007723, -24.83602698348160231, 1.605859176311266845 ) ) ;
#84191=CARTESIAN_POINT ( 'NONE',  ( 0.4224338394261131779, -19.80333402765648998, -1.500000000000002220 ) ) ;
#84193=ORIENTED_EDGE ( 'NONE', *, *, #30242, .T. ) ;
#84194=CARTESIAN_POINT ( 'NONE',  ( -2.359408512905806443, -20.17289352931189583, 11.49999999999999645 ) ) ;
#84195=CARTESIAN_POINT ( 'NONE',  ( -80.53629819409418644, -25.00158670708910691, 2.256160236439221034 ) ) ;
#84199=B_SPLINE_SURFACE_WITH_KNOTS ( 'NONE', 3, 1, ( 
 ( #47799, #9222 ),
 ( #27468, #3140 ),
 ( #33575, #18348 ),
 ( #4628, #34582 ),
 ( #49821, #96467 ),
 ( #95469, #64553 ),
 ( #25957, #35078 ),
 ( #41704, #26957 ),
 ( #19826, #96969 ),
 ( #4127, #74623 ),
 ( #66050, #58427 ),
 ( #57931, #82236 ),
 ( #34082, #95970 ),
 ( #88362, #49315 ),
 ( #56929, #73145 ),
 ( #43683, #72646 ),
 ( #89856, #12716 ),
 ( #3633, #80753 ),
 ( #89359, #35580 ) ),
 .UNSPECIFIED., .F., .F., .F.,
 ( 4, 1, 1, 1, 1, 1, 1, 1, 1, 1, 1, 1, 1, 1, 1, 1, 4 ),
 ( 2, 2 ),
 ( 0.000000000000000000, 0.07655893299405017172, 0.1491613519791141207, 0.2188268461269970711, 0.2855671390889793493, 0.3503131057192113151, 0.4141251538580798530, 0.4771791613162286727, 0.5403680185081830567, 0.6022023899907512634, 0.6620336537315649750, 0.7199344070495802272, 0.7759074326823265366, 0.8311148643832972915, 0.8866674470119635387, 0.9425523618334878950, 1.000000000000000000 ),
 ( 0.000000000000000000, 1.000000000000000000 ),
 .UNSPECIFIED. ) ;
#84200=CARTESIAN_POINT ( 'NONE',  ( -102.5550590363431525, -23.96169478059713853, 10.65365249895717881 ) ) ;
#84201=CARTESIAN_POINT ( 'NONE',  ( -62.55620429048337883, -24.64898659630528144, 1.056161002820822370 ) ) ;
#84202=CARTESIAN_POINT ( 'NONE',  ( -48.88506298778586512, -25.31602037465095023, 5.954471470684543633 ) ) ;
#84203=CARTESIAN_POINT ( 'NONE',  ( -40.57795224265260714, -24.83644354573577928, 8.397322867130096569 ) ) ;
#84204=DIRECTION ( 'NONE',  ( 1.000000000000000000, 3.773278334444167608E-23, 8.201307809403802430E-29 ) ) ;
#84205=CARTESIAN_POINT ( 'NONE',  ( -10.42242239376218116, -17.14354752861867937, -1.500000000000002220 ) ) ;
#84209=CARTESIAN_POINT ( 'NONE',  ( 21.34038654641452482, 8.310931564070170197, 11.49999999999999645 ) ) ;
#84210=CARTESIAN_POINT ( 'NONE',  ( -20.46125754976198508, 9.905080999540670561, -1.500000000000002220 ) ) ;
#84211=CARTESIAN_POINT ( 'NONE',  ( -49.53524246831344868, -25.31297094192622055, 4.168640163678797528 ) ) ;
#84212=CARTESIAN_POINT ( 'NONE',  ( -50.92287095715005307, -23.47596703998600631, 11.44779298504227683 ) ) ;
#84213=CARTESIAN_POINT ( 'NONE',  ( -59.62287095715002039, -24.33832256526968507, 0.1851278514119832352 ) ) ;
#84216=EDGE_CURVE ( 'NONE', #58299, #3088, #92622, .T. ) ;
#84217=ADVANCED_FACE ( 'NONE', ( #99747 ), #16520, .T. ) ;
#84218=CARTESIAN_POINT ( 'NONE',  ( -118.6228709571501128, -24.35013146730204525, 9.818937971375097717 ) ) ;
#84222=CARTESIAN_POINT ( 'NONE',  ( -9.871001836803966256, -17.81128643866572148, 11.49999999999998934 ) ) ;
#84224=CARTESIAN_POINT ( 'NONE',  ( 12.10309942457327992, -19.51426552955538085, 11.49999999999998934 ) ) ;
#84227=VERTEX_POINT ( 'NONE', #47490 ) ;
#84229=CARTESIAN_POINT ( 'NONE',  ( -38.62287095715004881, -23.94994826722515668, -0.6494450866351730856 ) ) ;
#84230=CARTESIAN_POINT ( 'NONE',  ( -77.60588210490597305, -23.48786465467240703, 11.44779295918254647 ) ) ;
#84232=CARTESIAN_POINT ( 'NONE',  ( -51.53636606068200621, -24.51419770103156637, 9.386484678747175181 ) ) ;
#84233=CARTESIAN_POINT ( 'NONE',  ( 20.00388196354723291, 7.160935007556333609, 11.49999999999999645 ) ) ;
#84237=CARTESIAN_POINT ( 'NONE',  ( 22.20243239366838850, -0.07139729354238147363, 11.49999999999998934 ) ) ;
#84238=CARTESIAN_POINT ( 'NONE',  ( -4.647353109605855792, 20.10343637636090719, -1.500000000000002220 ) ) ;
#84239=VECTOR ( 'NONE', #50482, 1000.000000000000114 ) ;
#84241=EDGE_LOOP ( 'NONE', ( #31454, #97003, #26623, #48470 ) ) ;
#84242=CARTESIAN_POINT ( 'NONE',  ( -109.4178292903974352, -25.27682816490595386, 5.278454515681120895 ) ) ;
#84243=CARTESIAN_POINT ( 'NONE',  ( -39.58139524285506639, -25.16756951564716260, 3.109746001908771262 ) ) ;
#84245=CARTESIAN_POINT ( 'NONE',  ( -51.62287095715003460, -24.51387760970725083, 9.387446482453428942 ) ) ;
#84246=ORIENTED_EDGE ( 'NONE', *, *, #55296, .T. ) ;
#84249=CARTESIAN_POINT ( 'NONE',  ( -88.52287095715009002, -24.66019654487200441, 8.947790411086119278 ) ) ;
#84250=CARTESIAN_POINT ( 'NONE',  ( 18.01467621842780176, -10.50282939286117667, -1.500000000000002220 ) ) ;
#84251=ADVANCED_FACE ( 'NONE', ( #76418 ), #55671, .T. ) ;
#84252=CARTESIAN_POINT ( 'NONE',  ( -13.65724274058436194, -16.95215541261048742, 11.49999999999999645 ) ) ;
#84253=DIRECTION ( 'NONE',  ( -3.773278334453079030E-23, 0.9999999999976377785, 2.173523156925979128E-06 ) ) ;
#84254=CARTESIAN_POINT ( 'NONE',  ( -78.51706125329930330, -23.73791477778911840, 11.05961554403170588 ) ) ;
#84255=CARTESIAN_POINT ( 'NONE',  ( 3.503984654965784706, -22.18958196551723816, 11.49999999999998934 ) ) ;
#84257=VERTEX_POINT ( 'NONE', #68330 ) ;
#84260=B_SPLINE_CURVE_WITH_KNOTS ( 'NONE', 3,
 ( #51816, #38071, #61429, #52312, #44699, #59936 ),
 .UNSPECIFIED., .F., .F.,
 ( 4, 2, 4 ),
 ( 1.570755371633974110E-05, 0.001396183895866088187, 0.002776660238015836880 ),
 .UNSPECIFIED. ) ;
#84261=VERTEX_POINT ( 'NONE', #62225 ) ;
#84266=B_SPLINE_CURVE_WITH_KNOTS ( 'NONE', 3,
 ( #25216, #77987, #63307, #888, #94226, #40458 ),
 .UNSPECIFIED., .F., .F.,
 ( 4, 2, 4 ),
 ( 6.391158118970787649E-06, 0.001387004593080793302, 0.002767618028042615873 ),
 .UNSPECIFIED. ) ;
#84267=CARTESIAN_POINT ( 'NONE',  ( 7.684279652734260502, -19.92951104315265809, -1.500000000000002220 ) ) ;
#84270=CARTESIAN_POINT ( 'NONE',  ( -0.5131542516139314669, 21.03015271272555253, -1.500000000000002220 ) ) ;
#84271=CARTESIAN_POINT ( 'NONE',  ( -30.54636096246643007, -24.57768521104549464, 0.8299800598022480935 ) ) ;
#84272=CARTESIAN_POINT ( 'NONE',  ( -99.52886026165788280, -25.25974063076742127, 3.946325710025691436 ) ) ;
#84273=CARTESIAN_POINT ( 'NONE',  ( -65.52287095715007581, -24.62285846331437966, 9.038163153548230966 ) ) ;
#84274=CARTESIAN_POINT ( 'NONE',  ( 21.96865551644221881, -1.217672407684077918, -1.500000000000002220 ) ) ;
#84275=CARTESIAN_POINT ( 'NONE',  ( -87.62358872278186084, -24.65952944569305316, 1.056160979905705455 ) ) ;
#84276=ORIENTED_EDGE ( 'NONE', *, *, #9322, .F. ) ;
#84277=LINE ( 'NONE', #54849, #69688 ) ;
#84283=CARTESIAN_POINT ( 'NONE',  ( -12.14505723179402530, 17.47690347785001919, 11.49999999999998934 ) ) ;
#84284=CARTESIAN_POINT ( 'NONE',  ( -68.62287095715005592, -29.50250243563736774, 8.947779886222143375 ) ) ;
#84285=CARTESIAN_POINT ( 'NONE',  ( -107.5502766971892470, -24.51419770103159124, 9.386484678747168076 ) ) ;
#84288=FACE_OUTER_BOUND ( 'NONE', #82741, .T. ) ;
#84289=CARTESIAN_POINT ( 'NONE',  ( -11.50411854321151672, 19.32100693743031528, -1.500000000000002220 ) ) ;
#84290=CARTESIAN_POINT ( 'NONE',  ( -109.9100400679505611, -25.06174035403189038, 7.474877196992075312 ) ) ;
#84293=CARTESIAN_POINT ( 'NONE',  ( -0.6043519431218743465, -19.59835197619436187, 11.49999999999999645 ) ) ;
#84294=CARTESIAN_POINT ( 'NONE',  ( -61.64687923781919920, -25.14083923594766645, 2.947789366383931853 ) ) ;
#84297=CARTESIAN_POINT ( 'NONE',  ( -68.94623785908815705, -25.26418252652374719, 6.008735871699613540 ) ) ;
#84298=CARTESIAN_POINT ( 'NONE',  ( -125.7765793602851119, -25.31364603714071748, 6.500954295741695255 ) ) ;
#84299=CARTESIAN_POINT ( 'NONE',  ( -124.6238243596118167, -24.51419770103158768, 9.386484678747164523 ) ) ;
#84300=CARTESIAN_POINT ( 'NONE',  ( -50.62287095715005592, -23.47593901973091235, -1.443836447539009749 ) ) ;
#84301=CARTESIAN_POINT ( 'NONE',  ( -2.117704968268854682, 19.61795684621070990, -1.500000000000002220 ) ) ;
#84302=AXIS2_PLACEMENT_3D ( 'NONE', #77254, #59200, #53951 ) ;
#84308=VECTOR ( 'NONE', #14537, 1000.000000000000227 ) ;
#84309=ADVANCED_FACE ( 'NONE', ( #63739 ), #15084, .T. ) ;
#84311=EDGE_CURVE ( 'NONE', #11314, #9142, #20026, .T. ) ;
#84314=CARTESIAN_POINT ( 'NONE',  ( -96.62287095715005592, -29.50250786944525672, 11.44777988621623166 ) ) ;
#84315=CARTESIAN_POINT ( 'NONE',  ( -55.49534339757938284, -24.40034930558990922, 0.3402023900116048494 ) ) ;
#84316=CARTESIAN_POINT ( 'NONE',  ( -99.48801098274306298, -25.26638478602427540, 7.273530140502286301 ) ) ;
#84318=CARTESIAN_POINT ( 'NONE',  ( -109.6228709571500559, -29.50250243563736774, 8.947779886222136270 ) ) ;
#84319=CARTESIAN_POINT ( 'NONE',  ( -112.5228709571500758, -23.72747288104470087, -1.053458166803225238 ) ) ;
#84320=CARTESIAN_POINT ( 'NONE',  ( 8.874027960929927517, 17.90919871486395465, 11.49999999999998934 ) ) ;
#84321=CARTESIAN_POINT ( 'NONE',  ( -125.6228709571500559, -23.85229601348998330, 10.88205029486206499 ) ) ;
#84322=CARTESIAN_POINT ( 'NONE',  ( -45.56056934063202846, -23.85049219812685095, 10.88485053497527133 ) ) ;
#84323=ORIENTED_EDGE ( 'NONE', *, *, #24132, .T. ) ;
#84324=CARTESIAN_POINT ( 'NONE',  ( -66.52287095715009002, -24.51283580621365843, 0.6167428607019661557 ) ) ;
#84327=CARTESIAN_POINT ( 'NONE',  ( -81.63319430079627637, -24.15543982623907482, -0.2315651400026469686 ) ) ;
#84328=CARTESIAN_POINT ( 'NONE',  ( -28.13975365244298388, -25.26026296467510335, 1.675769660708008590 ) ) ;
#84332=CARTESIAN_POINT ( 'NONE',  ( -91.52287095715006160, -29.50248528299804818, 1.056150453629040253 ) ) ;
#84333=VERTEX_POINT ( 'NONE', #2326 ) ;
#84334=CARTESIAN_POINT ( 'NONE',  ( -9.609455416251792670, -17.83980533922896683, 11.49999999999998934 ) ) ;
#84335=EDGE_CURVE ( 'NONE', #53188, #50179, #4215, .T. ) ;
#84336=CARTESIAN_POINT ( 'NONE',  ( -61.52287095715009002, -24.33832256527048798, 0.1851278514138564868 ) ) ;
#84337=CARTESIAN_POINT ( 'NONE',  ( -49.62287095715005592, -23.48783264082478084, -1.443836473390070596 ) ) ;
#84338=EDGE_CURVE ( 'NONE', #15988, #53767, #26147, .T. ) ;
#84339=EDGE_CURVE ( 'NONE', #90885, #61887, #88555, .T. ) ;
#84340=CARTESIAN_POINT ( 'NONE',  ( -83.58953762381672448, -23.48783264082478794, -1.443836473390065711 ) ) ;
#84341=EDGE_CURVE ( 'NONE', #77364, #38437, #70829, .T. ) ;
#84343=LINE ( 'NONE', #91453, #93934 ) ;
#84344=CARTESIAN_POINT ( 'NONE',  ( -61.92287095715006728, -23.47596703998600631, 11.44779298504227683 ) ) ;
#84345=CARTESIAN_POINT ( 'NONE',  ( -3.374260732160392795, -19.82512954709321562, -1.500000000000002220 ) ) ;
#84346=CARTESIAN_POINT ( 'NONE',  ( -17.90976863334866920, 11.11529090135583075, 11.49999999999999645 ) ) ;
#84347=ADVANCED_FACE ( 'NONE', ( #73333 ), #91906, .T. ) ;
#84348=DIRECTION ( 'NONE',  ( -3.773278334453080206E-23, 0.9999999999976377785, 2.173523156925979975E-06 ) ) ;
#84349=CARTESIAN_POINT ( 'NONE',  ( 10.71795340210964120, -19.33932934982082585, -1.500000000000002220 ) ) ;
#84351=CARTESIAN_POINT ( 'NONE',  ( 20.20254288951482735, -3.758238384022974277, 11.49999999999998934 ) ) ;
#84352=CARTESIAN_POINT ( 'NONE',  ( -96.52287095715001897, -23.94994826722564696, -0.6494450866342700301 ) ) ;
#84353=CARTESIAN_POINT ( 'NONE',  ( -60.53292719975349456, -24.83618233451449697, 1.606449574219535936 ) ) ;
#84354=VERTEX_POINT ( 'NONE', #7170 ) ;
#84355=DIRECTION ( 'NONE',  ( -3.773278334453079618E-23, 0.9999999999976377785, 2.173523156925979975E-06 ) ) ;
#84356=EDGE_LOOP ( 'NONE', ( #65317, #25645, #74700, #11036 ) ) ;
#84358=B_SPLINE_CURVE_WITH_KNOTS ( 'NONE', 3,
 ( #46857, #68199, #53488, #92023, #45860, #14892, #77779, #76778 ),
 .UNSPECIFIED., .F., .F.,
 ( 4, 2, 2, 4 ),
 ( 0.000000000000000000, 0.002001079623178218889, 0.003001619434767332454, 0.004002159246356446452 ),
 .UNSPECIFIED. ) ;
#84359=CARTESIAN_POINT ( 'NONE',  ( -87.52287095715006160, -24.66019654487200086, 8.947790411086115725 ) ) ;
#84360=ORIENTED_EDGE ( 'NONE', *, *, #70749, .T. ) ;
#84362=B_SPLINE_CURVE_WITH_KNOTS ( 'NONE', 3,
 ( #34196, #73258, #65169, #56544, #872, #8483 ),
 .UNSPECIFIED., .F., .F.,
 ( 4, 2, 4 ),
 ( 0.000000000000000000, 0.001380764517854765182, 0.002761529035709530365 ),
 .UNSPECIFIED. ) ;
#84363=VERTEX_POINT ( 'NONE', #68087 ) ;
#84364=CARTESIAN_POINT ( 'NONE',  ( -65.58953762381672448, -23.48783264082478084, -1.443836473390067265 ) ) ;
#84365=CARTESIAN_POINT ( 'NONE',  ( -49.28933921805457885, -25.11422830839963183, 7.151346021204567194 ) ) ;
#84367=CARTESIAN_POINT ( 'NONE',  ( 14.23986175545555355, -14.96101607593195304, -1.500000000000002220 ) ) ;
#84368=EDGE_CURVE ( 'NONE', #69591, #47870, #69631, .T. ) ;
#84369=EDGE_CURVE ( 'NONE', #35109, #69268, #28459, .T. ) ;
#84370=CARTESIAN_POINT ( 'NONE',  ( -0.6006773669993965559, 21.62980403441659760, 11.49999999999999645 ) ) ;
#84371=VERTEX_POINT ( 'NONE', #42399 ) ;
#84372=CARTESIAN_POINT ( 'NONE',  ( -116.4728709571500502, -29.48149383318413896, 5.000941583504024734 ) ) ;
#84374=CARTESIAN_POINT ( 'NONE',  ( -19.80502325505778671, 10.42642913751328670, -1.500000000000002220 ) ) ;
#84375=CARTESIAN_POINT ( 'NONE',  ( -79.60383831484530504, -25.27875002055017717, 6.693228756426554682 ) ) ;
#84376=CARTESIAN_POINT ( 'NONE',  ( -84.58831393107031715, -24.34968618360934300, 0.1864209137778835568 ) ) ;
#84380=CARTESIAN_POINT ( 'NONE',  ( -49.63954908479055206, -24.15620529776627379, 10.23563542870661003 ) ) ;
#84382=CARTESIAN_POINT ( 'NONE',  ( -27.70544111104076990, -24.61528742064533049, 1.628749860405701799 ) ) ;
#84383=CARTESIAN_POINT ( 'NONE',  ( -9.975069251262826953, -18.38325097723136992, 11.49999999999998934 ) ) ;
#84385=CARTESIAN_POINT ( 'NONE',  ( -67.51596021373018175, -23.73791477778911840, 11.05961554403170766 ) ) ;
#84386=EDGE_CURVE ( 'NONE', #73893, #16766, #74482, .T. ) ;
#84387=ORIENTED_EDGE ( 'NONE', *, *, #2471, .F. ) ;
#84388=ORIENTED_EDGE ( 'NONE', *, *, #77247, .T. ) ;
#84389=CARTESIAN_POINT ( 'NONE',  ( -50.62287095715009144, -24.62285846362214059, 9.038163152653526211 ) ) ;
#84390=CARTESIAN_POINT ( 'NONE',  ( 12.09327641706010326, 17.40255341615222306, -1.500000000000002220 ) ) ;
#84392=ORIENTED_EDGE ( 'NONE', *, *, #70413, .F. ) ;
#84394=DIRECTION ( 'NONE',  ( -0.000000000000000000, 2.173523156925979552E-06, -0.9999999999976378895 ) ) ;
#84395=CARTESIAN_POINT ( 'NONE',  ( 18.19902423439809525, 11.99547645517801442, -1.500000000000002220 ) ) ;
#84396=CARTESIAN_POINT ( 'NONE',  ( -32.52287095715006160, -29.50250243563736774, 8.947779886222150481 ) ) ;
#84397=CARTESIAN_POINT ( 'NONE',  ( -36.62287095715005592, -23.47593901973091235, -1.443836447539011525 ) ) ;
#84399=CARTESIAN_POINT ( 'NONE',  ( -6.661741538832703036, 20.79550341630197607, -1.500000000000002220 ) ) ;
#84400=CARTESIAN_POINT ( 'NONE',  ( -78.98851047203717712, -25.23623852701372883, 6.393657086652656751 ) ) ;
#84401=ORIENTED_EDGE ( 'NONE', *, *, #59093, .F. ) ;
#84402=CARTESIAN_POINT ( 'NONE',  ( -41.62287095715006302, -23.72747288104469732, -1.053458166803227458 ) ) ;
#84406=EDGE_LOOP ( 'NONE', ( #84901, #58517, #67983, #61682 ) ) ;
#84407=EDGE_CURVE ( 'NONE', #7353, #38251, #63533, .T. ) ;
#84408=ORIENTED_EDGE ( 'NONE', *, *, #98122, .T. ) ;
#84409=EDGE_CURVE ( 'NONE', #833, #27644, #22381, .T. ) ;
#84412=CARTESIAN_POINT ( 'NONE',  ( -17.78888362263414535, -11.56919986243916654, -1.500000000000002220 ) ) ;
#84413=CARTESIAN_POINT ( 'NONE',  ( -94.62789440740766622, -24.34968618360933945, 0.1864209137778861103 ) ) ;
#84414=CARTESIAN_POINT ( 'NONE',  ( -78.99318656846928377, -25.03138047770763208, 6.404755157858139647 ) ) ;
#84415=CARTESIAN_POINT ( 'NONE',  ( -28.52287095715005805, -23.32378116302990279, 11.44779301262222049 ) ) ;
#84417=CARTESIAN_POINT ( 'NONE',  ( -19.00951991574052968, 3.723548053296564575, 11.49999999999998934 ) ) ;
#84418=ADVANCED_FACE ( 'NONE', ( #38119 ), #89055, .F. ) ;
#84419=CARTESIAN_POINT ( 'NONE',  ( -40.93620634839454908, -25.20650829394578096, 6.812666491500989352 ) ) ;
#84420=ORIENTED_EDGE ( 'NONE', *, *, #69765, .F. ) ;
#84421=CARTESIAN_POINT ( 'NONE',  ( 18.80106323769845389, 4.952424739525837616, 11.49999999999999645 ) ) ;
#84423=ORIENTED_EDGE ( 'NONE', *, *, #61849, .T. ) ;
#84427=CARTESIAN_POINT ( 'NONE',  ( -93.64042061265114114, -23.48786465467241058, 11.44779295918254469 ) ) ;
#84428=CARTESIAN_POINT ( 'NONE',  ( -2.340448316220725467, 19.49152957720520618, -1.500000000000002220 ) ) ;
#84429=CARTESIAN_POINT ( 'NONE',  ( -41.46533095918948675, -25.27805952104409215, 4.218578510459923159 ) ) ;
#84430=ORIENTED_EDGE ( 'NONE', *, *, #5, .T. ) ;
#84431=CARTESIAN_POINT ( 'NONE',  ( 17.62533924669398999, -12.40915598911231577, -1.500000000000002220 ) ) ;
#84432=CARTESIAN_POINT ( 'NONE',  ( -33.52200571196073042, -23.48786465467240347, 11.44779295918255535 ) ) ;
#84433=LINE ( 'NONE', #4091, #68528 ) ;
#84435=CARTESIAN_POINT ( 'NONE',  ( -78.22287095715005023, -23.47593901973090169, -1.443836447538997092 ) ) ;
#84436=CARTESIAN_POINT ( 'NONE',  ( -22.27228905017084060, 5.866681652885556986, -1.500000000000002220 ) ) ;
#84438=CARTESIAN_POINT ( 'NONE',  ( -93.63681820332803341, -23.73766607897670511, -1.055555164236453791 ) ) ;
#84440=CARTESIAN_POINT ( 'NONE',  ( 19.72175082351460063, -4.362005935662174316, 11.49999999999999645 ) ) ;
#84441=CARTESIAN_POINT ( 'NONE',  ( -126.5562042904833930, -23.48783264082479150, -1.443836473390057273 ) ) ;
#84443=CARTESIAN_POINT ( 'NONE',  ( -110.4629859055347936, -25.29823811875587225, 2.835693564650067611 ) ) ;
#84446=CARTESIAN_POINT ( 'NONE',  ( 14.98761344906185577, -13.09354923471379983, 11.49999999999998934 ) ) ;
#84447=FACE_OUTER_BOUND ( 'NONE', #11035, .T. ) ;
#84448=CARTESIAN_POINT ( 'NONE',  ( 16.35176858736616978, 11.14859404531058473, -1.500000000000002220 ) ) ;
#84449=CARTESIAN_POINT ( 'NONE',  ( -56.62787117652145241, -24.51314013834315730, 0.6176544820404098468 ) ) ;
#84450=VECTOR ( 'NONE', #44395, 1000.000000000000114 ) ;
#84452=DIRECTION ( 'NONE',  ( -1.000000000000000000, -3.773278334444167608E-23, -8.201307833595939069E-29 ) ) ;
#84454=CARTESIAN_POINT ( 'NONE',  ( -6.358105417860958397, -19.66046682221446318, 11.49999999999999645 ) ) ;
#84456=CARTESIAN_POINT ( 'NONE',  ( -106.6321223050444900, -23.73766607897671577, -1.055555164236449572 ) ) ;
#84457=CARTESIAN_POINT ( 'NONE',  ( 15.30562342774392093, -16.77826389816909725, 11.49999999999999645 ) ) ;
#84458=EDGE_LOOP ( 'NONE', ( #92235, #80720, #58460, #78384 ) ) ;
#84460=CARTESIAN_POINT ( 'NONE',  ( -93.62287095715005592, -24.65952944569304606, 1.056160979905701236 ) ) ;
#84464=CARTESIAN_POINT ( 'NONE',  ( -5.623992922573770592, 19.38241096367466199, 11.49999999999998934 ) ) ;
#84465=B_SPLINE_CURVE_WITH_KNOTS ( 'NONE', 3,
 ( #65031, #2612, #95944, #57410 ),
 .UNSPECIFIED., .F., .F.,
 ( 4, 4 ),
 ( 0.000000000000000000, 0.0009166666666666628549 ),
 .UNSPECIFIED. ) ;
#84467=EDGE_CURVE ( 'NONE', #21835, #66467, #1886, .T. ) ;
#84468=CARTESIAN_POINT ( 'NONE',  ( -95.62287095715007013, -23.84047902841601996, -0.8780736468305821996 ) ) ;
#84470=VERTEX_POINT ( 'NONE', #31011 ) ;
#84471=EDGE_CURVE ( 'NONE', #16750, #48546, #7794, .T. ) ;
#84474=CARTESIAN_POINT ( 'NONE',  ( -16.32851894532483783, 16.03542138455653898, 11.49999999999998934 ) ) ;
#84475=CARTESIAN_POINT ( 'NONE',  ( -102.6228709571500559, -29.50250243563736774, 8.947779886222138046 ) ) ;
#84476=CARTESIAN_POINT ( 'NONE',  ( -2.787017431591729988, -21.48445716988565835, -1.500000000000002220 ) ) ;
#84478=CARTESIAN_POINT ( 'NONE',  ( -34.64978355792892017, -23.96119346886880663, -0.6495511937831990323 ) ) ;
#84479=CARTESIAN_POINT ( 'NONE',  ( -7.158894406585330827, 19.61798520005962487, 11.49999999999999645 ) ) ;
#84482=FACE_OUTER_BOUND ( 'NONE', #62320, .T. ) ;
#84483=CARTESIAN_POINT ( 'NONE',  ( -14.32918165687622825, -16.72005635474405949, -1.500000000000002220 ) ) ;
#84484=CARTESIAN_POINT ( 'NONE',  ( -105.5468779439268587, -24.92592662359561473, 8.075495903018000021 ) ) ;
#84485=CARTESIAN_POINT ( 'NONE',  ( -40.50110916354886825, -25.10925768751217291, 2.834725980302106763 ) ) ;
#84486=EDGE_LOOP ( 'NONE', ( #56533, #27482, #9273, #91361 ) ) ;
#84488=CARTESIAN_POINT ( 'NONE',  ( -90.59505941600714607, -24.15602025860896873, 10.28564288303535434 ) ) ;
#84490=CARTESIAN_POINT ( 'NONE',  ( -93.22287095715005023, -23.47596703998600631, 11.44779298504227860 ) ) ;
#84492=VERTEX_POINT ( 'NONE', #23381 ) ;
#84493=CARTESIAN_POINT ( 'NONE',  ( -71.54133414514889466, -24.51419770103159124, 9.386484678747166299 ) ) ;
#84494=CARTESIAN_POINT ( 'NONE',  ( -101.7776484685884242, -25.10936053256603273, 3.986250973267613240 ) ) ;
#84496=CARTESIAN_POINT ( 'NONE',  ( -18.53176153473302179, -8.692061069824589481, -1.500000000000002220 ) ) ;
#84500=CARTESIAN_POINT ( 'NONE',  ( -44.51366543650918572, -23.73766607897669800, -1.055555164236459120 ) ) ;
#84502=CARTESIAN_POINT ( 'NONE',  ( 1.165341552704713513, 22.26021350444069213, 11.49999999999998934 ) ) ;
#84503=CARTESIAN_POINT ( 'NONE',  ( -80.64675904551151575, -25.20074414427590881, 3.409327697718777195 ) ) ;
#84506=ORIENTED_EDGE ( 'NONE', *, *, #66142, .F. ) ;
#84507=DIRECTION ( 'NONE',  ( -3.773278334453079030E-23, 0.9999999999976377785, 2.173523156925979128E-06 ) ) ;
#84508=CARTESIAN_POINT ( 'NONE',  ( -29.66400988275576367, -25.26247693264633654, 6.487135408686464544 ) ) ;
#84509=CARTESIAN_POINT ( 'NONE',  ( 5.313885144808909722, 20.14914662543312929, 11.49999999999998934 ) ) ;
#84510=ORIENTED_EDGE ( 'NONE', *, *, #18771, .T. ) ;
#84513=CARTESIAN_POINT ( 'NONE',  ( -51.21833214457227257, -25.25854513373207055, 6.843755114720857513 ) ) ;
#84514=VERTEX_POINT ( 'NONE', #46749 ) ;
#84515=VERTEX_POINT ( 'NONE', #24898 ) ;
#84516=PLANE ( 'NONE',  #88416 ) ;
#84517=CARTESIAN_POINT ( 'NONE',  ( -55.62287095715007013, -23.84081130438200091, 10.88220057463249191 ) ) ;
#84518=CARTESIAN_POINT ( 'NONE',  ( -110.2093792378192063, -25.30161501422653814, 5.585409209247975681 ) ) ;
#84520=CARTESIAN_POINT ( 'NONE',  ( -110.5228709571500332, -24.14321612903118464, -0.2833117244520817479 ) ) ;
#84522=CARTESIAN_POINT ( 'NONE',  ( 10.50125231818214289, 19.49540335892314502, 11.49999999999999645 ) ) ;
#84523=VERTEX_POINT ( 'NONE', #8183 ) ;
#84524=CARTESIAN_POINT ( 'NONE',  ( -78.62287095715005592, -24.64965695001468404, 8.947790433994182280 ) ) ;
#84525=CARTESIAN_POINT ( 'NONE',  ( -14.08738070862771963, 17.71811851510361535, 11.49999999999998934 ) ) ;
#84526=EDGE_CURVE ( 'NONE', #20835, #65831, #1582, .T. ) ;
#84527=CARTESIAN_POINT ( 'NONE',  ( -92.52287095715009002, -23.73907113217727272, -1.053371485780262296 ) ) ;
#84532=DIRECTION ( 'NONE',  ( -3.773278334453079030E-23, 0.9999999999976377785, 2.173523156925979128E-06 ) ) ;
#84534=CARTESIAN_POINT ( 'NONE',  ( -7.184633862932894743, 18.80532529184710100, 11.49999999999998934 ) ) ;
#84537=CARTESIAN_POINT ( 'NONE',  ( -39.55620429048340014, -23.48786465467240347, 11.44779295918255180 ) ) ;
#84538=CARTESIAN_POINT ( 'NONE',  ( 22.34790896907852442, -0.4833156648990815651, -1.500000000000002220 ) ) ;
#84539=VERTEX_POINT ( 'NONE', #62989 ) ;
#84541=CARTESIAN_POINT ( 'NONE',  ( -35.22287095715007155, -23.47593901973090169, -1.443836447538997980 ) ) ;
#84542=CARTESIAN_POINT ( 'NONE',  ( -82.62287095715005592, -29.50250786944525672, 11.44777988621623521 ) ) ;
#84544=CARTESIAN_POINT ( 'NONE',  ( -68.52287095715006160, -23.48786465467241058, 11.44779295918254647 ) ) ;
#84545=B_SPLINE_CURVE_WITH_KNOTS ( 'NONE', 3,
 ( #57146, #3362, #66761, #66263 ),
 .UNSPECIFIED., .F., .F.,
 ( 4, 4 ),
 ( 0.3407433164617006960, 0.3497497477338162297 ),
 .UNSPECIFIED. ) ;
#84546=CARTESIAN_POINT ( 'NONE',  ( -40.62287095715004170, -29.50248789122583659, 2.256150453626215580 ) ) ;
#84547=CARTESIAN_POINT ( 'NONE',  ( 15.26536572251939461, -12.21375333317339695, 11.49999999999998934 ) ) ;
#84549=CARTESIAN_POINT ( 'NONE',  ( -8.581294335678165908, -19.67629172487136557, 11.49999999999998934 ) ) ;
#84551=DIRECTION ( 'NONE',  ( -3.773278334453079618E-23, 0.9999999999976377785, 2.173523156925978705E-06 ) ) ;
#84553=CARTESIAN_POINT ( 'NONE',  ( -9.150087108448493822, 20.98025145036519845, -1.500000000000002220 ) ) ;
#84555=B_SPLINE_CURVE_WITH_KNOTS ( 'NONE', 3,
 ( #34923, #58757, #64404, #65404, #95322, #3981 ),
 .UNSPECIFIED., .F., .F.,
 ( 4, 2, 4 ),
 ( 3.102663313537988147E-09, 0.002226959955260804196, 0.004453916807858295489 ),
 .UNSPECIFIED. ) ;
#84557=CARTESIAN_POINT ( 'NONE',  ( -96.55485876771541598, -23.96169478059713498, 10.65365249895717881 ) ) ;
#84558=LINE ( 'NONE', #22642, #62059 ) ;
#84559=CARTESIAN_POINT ( 'NONE',  ( -19.95465934538571062, -0.7993260556091378310, 11.49999999999999645 ) ) ;
#84560=PLANE ( 'NONE',  #34875 ) ;
#84561=CARTESIAN_POINT ( 'NONE',  ( -124.6228709571500559, -23.48783264082479505, -1.443836473390058828 ) ) ;
#84565=CARTESIAN_POINT ( 'NONE',  ( -109.5228709571500616, -24.64898659630530275, 1.056161002820831474 ) ) ;
#84566=CARTESIAN_POINT ( 'NONE',  ( -59.52287095715006160, -29.50250786944525672, 11.44777988621623876 ) ) ;
#84567=CARTESIAN_POINT ( 'NONE',  ( -21.62197530259306788, 2.132803791230205359, 11.49999999999998934 ) ) ;
#84568=DIRECTION ( 'NONE',  ( -3.773278334453080206E-23, 0.9999999999976377785, 2.173523156925979975E-06 ) ) ;
#84569=CARTESIAN_POINT ( 'NONE',  ( -19.52990877098713796, 1.257015143768854815, -1.500000000000002220 ) ) ;
#84571=CARTESIAN_POINT ( 'NONE',  ( -40.52112337587701063, -25.18518878011527207, 3.295773480853921189 ) ) ;
#84573=CARTESIAN_POINT ( 'NONE',  ( -91.56188894598993500, -23.48786465467241413, 11.44779295918254469 ) ) ;
#84575=CARTESIAN_POINT ( 'NONE',  ( -14.38416181709762043, 14.64695106392160895, 11.49999999999999645 ) ) ;
#84576=CARTESIAN_POINT ( 'NONE',  ( -94.52287095715001897, -24.33832256527048088, 0.1851278514138636755 ) ) ;
#84578=LINE ( 'NONE', #90202, #38355 ) ;
#84579=EDGE_CURVE ( 'NONE', #43445, #8718, #40530, .T. ) ;
#84582=CARTESIAN_POINT ( 'NONE',  ( -109.3914004513356701, -25.29449945578133452, 4.479052194644536300 ) ) ;
#84584=CARTESIAN_POINT ( 'NONE',  ( -125.5541636680248274, -24.92592662359561828, 8.075495903018000021 ) ) ;
#84585=ADVANCED_FACE ( 'NONE', ( #41146 ), #27412, .T. ) ;
#84587=PLANE ( 'NONE',  #85642 ) ;
#84588=EDGE_CURVE ( 'NONE', #73442, #48696, #35027, .T. ) ;
#84589=CARTESIAN_POINT ( 'NONE',  ( -124.6228709571500701, -23.73934037231757799, 11.05740245334328087 ) ) ;
#84591=VECTOR ( 'NONE', #62259, 1000.000000000000114 ) ;
#84592=CARTESIAN_POINT ( 'NONE',  ( 17.08057647167376913, 15.47633299359885761, 11.49999999999999645 ) ) ;
#84593=CARTESIAN_POINT ( 'NONE',  ( -15.22011711465338912, -17.00649957279452451, 11.49999999999998934 ) ) ;
#84594=CARTESIAN_POINT ( 'NONE',  ( -104.5228709571500758, -24.64898659630529565, 1.056161002820829697 ) ) ;
#84595=ADVANCED_FACE ( 'NONE', ( #17800 ), #42156, .F. ) ;
#84596=CARTESIAN_POINT ( 'NONE',  ( -67.52287095715006160, -24.65952944569304961, 1.056160979905697239 ) ) ;
#84597=CARTESIAN_POINT ( 'NONE',  ( -58.87764846858842560, -25.13069340115296058, 2.947789388436138580 ) ) ;
#84599=CARTESIAN_POINT ( 'NONE',  ( 21.16571772479873204, -7.350578744355993344, 11.49999999999999645 ) ) ;
#84600=FACE_OUTER_BOUND ( 'NONE', #58086, .T. ) ;
#84601=EDGE_CURVE ( 'NONE', #50993, #55725, #53816, .T. ) ;
#84602=B_SPLINE_CURVE_WITH_KNOTS ( 'NONE', 3,
 ( #73801, #35251, #27639, #92013 ),
 .UNSPECIFIED., .F., .F.,
 ( 4, 4 ),
 ( 0.4601144809659691859, 0.4691209122380847751 ),
 .UNSPECIFIED. ) ;
#84603=CARTESIAN_POINT ( 'NONE',  ( -34.62287095715007013, -23.47596703998600276, 11.44779298504227505 ) ) ;
#84604=CARTESIAN_POINT ( 'NONE',  ( -8.017166757594178961, 20.41873492177044724, 11.49999999999998934 ) ) ;
#84608=LINE ( 'NONE', #37935, #92953 ) ;
#84609=PLANE ( 'NONE',  #27416 ) ;
#84610=ORIENTED_EDGE ( 'NONE', *, *, #19402, .F. ) ;
#84611=CARTESIAN_POINT ( 'NONE',  ( -17.80769721941407369, -10.09151516499986734, -1.500000000000002220 ) ) ;
#84612=ORIENTED_EDGE ( 'NONE', *, *, #71459, .T. ) ;
#84613=ORIENTED_EDGE ( 'NONE', *, *, #52862, .T. ) ;
#84614=EDGE_LOOP ( 'NONE', ( #70957, #7365, #21947, #98544 ) ) ;
#84616=CARTESIAN_POINT ( 'NONE',  ( -20.21456430084473155, -11.12997698910670152, 11.49999999999998934 ) ) ;
#84617=FACE_OUTER_BOUND ( 'NONE', #51058, .T. ) ;
#84618=CARTESIAN_POINT ( 'NONE',  ( 20.23688964843749005, 1.552196809742036221, -1.500000000000002220 ) ) ;
#84620=CARTESIAN_POINT ( 'NONE',  ( -28.21574693287574931, -24.80510216826755610, 2.243760839632586102 ) ) ;
#84621=CARTESIAN_POINT ( 'NONE',  ( -46.58953762381672448, -24.64898659630528499, 1.056161002820820372 ) ) ;
#84622=CARTESIAN_POINT ( 'NONE',  ( -126.6228709571500559, -29.50250243563736774, 8.947779886222132717 ) ) ;
#84623=CARTESIAN_POINT ( 'NONE',  ( -70.58659607870677632, -24.63355581998385091, 0.9682620441943861067 ) ) ;
#84624=CARTESIAN_POINT ( 'NONE',  ( 10.55508701655855575, -18.62573008410804221, 11.49999999999999645 ) ) ;
#84625=ORIENTED_EDGE ( 'NONE', *, *, #90093, .T. ) ;
#84627=CARTESIAN_POINT ( 'NONE',  ( -61.59281505598787021, -24.15620529776628089, 10.23563542870660825 ) ) ;
#84628=ORIENTED_EDGE ( 'NONE', *, *, #15046, .F. ) ;
#84629=CARTESIAN_POINT ( 'NONE',  ( -10.81534556030752725, -17.66751395530895152, -1.500000000000002220 ) ) ;
#84632=ORIENTED_EDGE ( 'NONE', *, *, #6844, .F. ) ;
#84634=B_SPLINE_SURFACE_WITH_KNOTS ( 'NONE', 3, 3, ( 
 ( #33170, #64151, #95075, #25560 ),
 ( #87461, #13815, #82832, #91947 ),
 ( #4728, #74718, #22417, #67142 ),
 ( #84327, #14313, #12818, #5716 ),
 ( #28548, #13315, #44294, #75711 ),
 ( #20427, #59023, #30038, #97567 ),
 ( #21422, #53403, #83836, #5220 ) ),
 .UNSPECIFIED., .F., .F., .F.,
 ( 4, 3, 4 ),
 ( 4, 4 ),
 ( 0.0004766839783841440902, 0.1029713700210908162, 0.2054660560637974753 ),
 ( 0.4896185478418259018, 0.4908571814961936175 ),
 .UNSPECIFIED. ) ;
#84635=CARTESIAN_POINT ( 'NONE',  ( -28.54454667017215641, -23.99501971000362843, -0.2315644524145782090 ) ) ;
#84637=ORIENTED_EDGE ( 'NONE', *, *, #74300, .F. ) ;
#84639=CARTESIAN_POINT ( 'NONE',  ( -65.51286458321119710, -23.85016227208580730, -0.8807180028928343063 ) ) ;
#84640=CARTESIAN_POINT ( 'NONE',  ( 8.537626919312410578, 20.26776412955123163, 11.49999999999999645 ) ) ;
#84641=CARTESIAN_POINT ( 'NONE',  ( -89.56219111058589988, -23.48786465467241413, 11.44779295918254292 ) ) ;
#84642=CARTESIAN_POINT ( 'NONE',  ( 3.584315319034878211, 22.25550262085195286, -1.500000000000002220 ) ) ;
#84643=B_SPLINE_CURVE_WITH_KNOTS ( 'NONE', 3,
 ( #27829, #74498, #3507, #34945, #96839, #50178 ),
 .UNSPECIFIED., .F., .F.,
 ( 4, 2, 4 ),
 ( 0.000000000000000000, 0.001380901958385392448, 0.002761803916770784895 ),
 .UNSPECIFIED. ) ;
#84644=CARTESIAN_POINT ( 'NONE',  ( -18.08314111433443827, -10.61732331186343004, 11.49999999999998934 ) ) ;
#84645=CARTESIAN_POINT ( 'NONE',  ( -111.6228709571500559, -24.64898659630368627, 1.056161002820831474 ) ) ;
#84648=AXIS2_PLACEMENT_3D ( 'NONE', #65269, #80459, #81469 ) ;
#84649=VERTEX_POINT ( 'NONE', #73094 ) ;
#84651=CARTESIAN_POINT ( 'NONE',  ( -36.62287095715005592, -23.48783264082477729, -1.443836473390072372 ) ) ;
#84653=CARTESIAN_POINT ( 'NONE',  ( -19.98823316618875268, 7.996883007359760320, -1.500000000000002220 ) ) ;
#84656=ORIENTED_EDGE ( 'NONE', *, *, #66279, .T. ) ;
#84657=CARTESIAN_POINT ( 'NONE',  ( -21.11812214938331422, 0.5215410354952813021, -1.500000000000002220 ) ) ;
#84658=CARTESIAN_POINT ( 'NONE',  ( -67.55620429048337883, -23.47593901973091235, -1.443836447539006196 ) ) ;
#84659=CARTESIAN_POINT ( 'NONE',  ( -130.5728709571500588, -23.47593901973090524, -1.443836447538995982 ) ) ;
#84660=CARTESIAN_POINT ( 'NONE',  ( -83.64500779952560094, -23.48786465467241413, 11.44779295918254469 ) ) ;
#84661=CARTESIAN_POINT ( 'NONE',  ( -32.52287095715006160, -29.50247984919015209, -1.443849546365062242 ) ) ;
#84662=CARTESIAN_POINT ( 'NONE',  ( -99.80419109892318374, -25.13411624585489434, 2.967105462742589239 ) ) ;
#84663=CARTESIAN_POINT ( 'NONE',  ( 4.116201370682176730, 21.75534844777131838, -1.500000000000002220 ) ) ;
#84664=CARTESIAN_POINT ( 'NONE',  ( -71.59237387687302601, -24.15543982623907127, -0.2315651400026636497 ) ) ;
#84667=LINE ( 'NONE', #100368, #65418 ) ;
#84671=CARTESIAN_POINT ( 'NONE',  ( 16.20606029192996900, -10.75321813762353251, 11.49999999999998934 ) ) ;
#84672=PLANE ( 'NONE',  #67398 ) ;
#84673=CARTESIAN_POINT ( 'NONE',  ( -18.60337119584764665, 10.53494341765418874, -1.500000000000002220 ) ) ;
#84674=CARTESIAN_POINT ( 'NONE',  ( -62.61044358207880123, -23.48783264082476308, -1.443836473390090580 ) ) ;
#84675=CARTESIAN_POINT ( 'NONE',  ( -106.5562042904834072, -23.48783264082478794, -1.443836473390061492 ) ) ;
#84676=CARTESIAN_POINT ( 'NONE',  ( -122.5228709571500616, -24.64965694238408034, 8.947790433994191162 ) ) ;
#84677=DIRECTION ( 'NONE',  ( 3.773278334444166432E-23, -1.000000000000000000, 0.000000000000000000 ) ) ;
#84678=CARTESIAN_POINT ( 'NONE',  ( 22.16846167567618053, -4.910139430472912458, -1.500000000000002220 ) ) ;
#84679=AXIS2_PLACEMENT_3D ( 'NONE', #73345, #87561, #49012 ) ;
#84680=CARTESIAN_POINT ( 'NONE',  ( -99.22287095715006444, -23.47596703998600276, 11.44779298504227860 ) ) ;
#84681=CARTESIAN_POINT ( 'NONE',  ( -127.6228709571500559, -24.65952944569305316, 1.056160979905707897 ) ) ;
#84682=CARTESIAN_POINT ( 'NONE',  ( -14.51517298184297289, -13.48802281452852725, 11.49999999999999645 ) ) ;
#84686=B_SPLINE_CURVE_WITH_KNOTS ( 'NONE', 3,
 ( #24886, #17281, #15772, #55864 ),
 .UNSPECIFIED., .F., .F.,
 ( 4, 4 ),
 ( 0.01050750315080129817, 0.01951393442291685446 ),
 .UNSPECIFIED. ) ;
#84688=CARTESIAN_POINT ( 'NONE',  ( -32.62287095715004881, -29.50250243563736774, 8.947779886222150481 ) ) ;
#84689=CARTESIAN_POINT ( 'NONE',  ( -5.517532219241116032, 20.92096086382833064, -1.500000000000002220 ) ) ;
#84691=CARTESIAN_POINT ( 'NONE',  ( 2.844571010020486845, -19.19604305453586690, -1.500000000000002220 ) ) ;
#84692=FACE_OUTER_BOUND ( 'NONE', #26467, .T. ) ;
#84693=DIRECTION ( 'NONE',  ( 1.000000000000000000, 3.773278334444166432E-23, 8.201307841325785021E-29 ) ) ;
#84694=CARTESIAN_POINT ( 'NONE',  ( 4.164567180745167185, 19.39263604865329071, -1.500000000000002220 ) ) ;
#84695=EDGE_LOOP ( 'NONE', ( #73211, #54311, #73515, #26235 ) ) ;
#84696=CARTESIAN_POINT ( 'NONE',  ( -16.58479117878708209, 11.75282063728064053, 11.49999999999999645 ) ) ;
#84698=CARTESIAN_POINT ( 'NONE',  ( -111.6228709571500559, -29.50250786944525672, 11.44777988621622988 ) ) ;
#84701=CARTESIAN_POINT ( 'NONE',  ( -0.04154859658887635060, -22.51212076658054428, 1.420893871182737023 ) ) ;
#84702=PLANE ( 'NONE',  #57420 ) ;
#84704=CARTESIAN_POINT ( 'NONE',  ( -128.6228709571499849, -23.73907113216991860, -1.053371485793219042 ) ) ;
#84706=CARTESIAN_POINT ( 'NONE',  ( -12.91570554291229023, -15.35452705144416896, -1.500000000000002220 ) ) ;
#84710=VERTEX_POINT ( 'NONE', #67979 ) ;
#84712=EDGE_CURVE ( 'NONE', #76106, #25473, #43048, .T. ) ;
#84713=CARTESIAN_POINT ( 'NONE',  ( 22.85676281555306844, 1.471244944367766649, 11.49999999999999645 ) ) ;
#84714=CARTESIAN_POINT ( 'NONE',  ( -13.58842472641693711, -18.21064416987719525, -1.500000000000002220 ) ) ;
#84715=EDGE_LOOP ( 'NONE', ( #53183, #68018, #60155, #56422 ) ) ;
#84717=AXIS2_PLACEMENT_3D ( 'NONE', #64767, #97673, #41399 ) ;
#84719=CARTESIAN_POINT ( 'NONE',  ( -28.52287095715007226, -23.32374950011072912, -1.443835813551990643 ) ) ;
#84722=CARTESIAN_POINT ( 'NONE',  ( -71.62287095715005592, -24.64898659630528854, 1.056161002820824368 ) ) ;
#84724=DIRECTION ( 'NONE',  ( -0.000000000000000000, 2.173523156925979552E-06, -0.9999999999976378895 ) ) ;
#84725=VERTEX_POINT ( 'NONE', #82184 ) ;
#84726=CARTESIAN_POINT ( 'NONE',  ( 20.34676669208793953, -0.1217515720461415790, -1.500000000000002220 ) ) ;
#84727=ORIENTED_EDGE ( 'NONE', *, *, #40866, .T. ) ;
#84728=EDGE_CURVE ( 'NONE', #68982, #94726, #90803, .T. ) ;
#84729=CARTESIAN_POINT ( 'NONE',  ( 12.94906671069258763, 19.00495796004926419, 11.49999999999998934 ) ) ;
#84730=CARTESIAN_POINT ( 'NONE',  ( -54.51465898514846486, -23.73791477778911485, 11.05961554403171121 ) ) ;
#84732=CARTESIAN_POINT ( 'NONE',  ( -108.5492781676227594, -24.66019654487200086, 8.947790411086106843 ) ) ;
#84733=DIRECTION ( 'NONE',  ( -3.773278334453079618E-23, 0.9999999999976377785, 2.173523156925979975E-06 ) ) ;
#84734=B_SPLINE_CURVE_WITH_KNOTS ( 'NONE', 3,
 ( #89556, #6803, #81938, #97169 ),
 .UNSPECIFIED., .F., .F.,
 ( 4, 4 ),
 ( 0.1005718158719557526, 0.1095782471440711753 ),
 .UNSPECIFIED. ) ;
#84735=VECTOR ( 'NONE', #3234, 1000.000000000000114 ) ;
#84736=CARTESIAN_POINT ( 'NONE',  ( -51.49549738738706850, -24.35071581493542681, 9.817618358456028815 ) ) ;
#84737=CARTESIAN_POINT ( 'NONE',  ( -6.410030533929251817, 20.24415959294862333, 11.49999999999999645 ) ) ;
#84738=ORIENTED_EDGE ( 'NONE', *, *, #35904, .T. ) ;
#84740=ORIENTED_EDGE ( 'NONE', *, *, #53757, .T. ) ;
#84741=CARTESIAN_POINT ( 'NONE',  ( 14.71430157977438924, -16.63553917435140406, 11.49999999999998934 ) ) ;
#84742=CARTESIAN_POINT ( 'NONE',  ( -9.157874670058189892, -18.46812626297970539, 11.49999999999998934 ) ) ;
#84745=VERTEX_POINT ( 'NONE', #84179 ) ;
#84746=CARTESIAN_POINT ( 'NONE',  ( -103.5228709571500758, -29.50248528299804818, 1.056150453629042030 ) ) ;
#84749=CARTESIAN_POINT ( 'NONE',  ( -91.64132767522438883, -23.48783264082477018, -1.443836473390090802 ) ) ;
#84750=VERTEX_POINT ( 'NONE', #51749 ) ;
#84752=CARTESIAN_POINT ( 'NONE',  ( -126.8949125657483421, -25.24693556693654273, 3.801660433955577290 ) ) ;
#84753=CARTESIAN_POINT ( 'NONE',  ( -44.52287095715006160, -23.72747288104469732, -1.053458166803227902 ) ) ;
#84754=CARTESIAN_POINT ( 'NONE',  ( 19.92439739378097840, -5.974006126113303949, -1.500000000000002220 ) ) ;
#84755=CARTESIAN_POINT ( 'NONE',  ( -4.706806674773570620, -21.25045708977441450, 11.49999999999999645 ) ) ;
#84758=CARTESIAN_POINT ( 'NONE',  ( -21.13723655771239152, -7.639886366525781014, 11.49999999999998934 ) ) ;
#84761=ORIENTED_EDGE ( 'NONE', *, *, #32492, .T. ) ;
#84763=CARTESIAN_POINT ( 'NONE',  ( -69.52287095715009002, -23.72773821059536914, 11.05748984161097326 ) ) ;
#84764=B_SPLINE_SURFACE_WITH_KNOTS ( 'NONE', 3, 3, ( 
 ( #67699, #12387, #96626, #43360 ),
 ( #5777, #11401, #4788, #74781 ),
 ( #3802, #5279, #36239, #67201 ),
 ( #98114, #27128, #58093, #50465 ),
 ( #28620, #59584, #90514, #13378 ),
 ( #68184, #61582, #75776, #13879 ),
 ( #45844, #38217, #85388, #658 ) ),
 .UNSPECIFIED., .F., .F., .F.,
 ( 4, 3, 4 ),
 ( 4, 4 ),
 ( 0.7945040050992244751, 0.8970133687736503436, 0.9995227324480761011 ),
 ( 0.5396311249913389174, 0.5408929790830778739 ),
 .UNSPECIFIED. ) ;
#84765=VERTEX_POINT ( 'NONE', #14669 ) ;
#84768=ORIENTED_EDGE ( 'NONE', *, *, #87711, .F. ) ;
#84769=CARTESIAN_POINT ( 'NONE',  ( 20.65877813657638740, 5.380652674160894655, -1.500000000000002220 ) ) ;
#84771=CARTESIAN_POINT ( 'NONE',  ( -17.33045254171255678, -11.89390297951003816, 11.49999999999998934 ) ) ;
#84772=CARTESIAN_POINT ( 'NONE',  ( -30.48808003178038462, -24.57318328807190966, 0.8299800598022502029 ) ) ;
#84773=CARTESIAN_POINT ( 'NONE',  ( -41.46524908126663433, -25.28892609849224016, 4.157779739328558932 ) ) ;
#84775=CARTESIAN_POINT ( 'NONE',  ( -11.46427080702723522, -18.74017919159951973, -1.500000000000002220 ) ) ;
#84776=CARTESIAN_POINT ( 'NONE',  ( -76.52287095715007581, -24.65952944569304606, 1.056160979905698794 ) ) ;
#84777=EDGE_LOOP ( 'NONE', ( #45196, #32577, #74054, #82965 ) ) ;
#84778=FACE_OUTER_BOUND ( 'NONE', #64182, .T. ) ;
#84780=CARTESIAN_POINT ( 'NONE',  ( -96.52287095715006160, -24.64898659630528499, 1.056161002820829697 ) ) ;
#84783=CARTESIAN_POINT ( 'NONE',  ( -130.5728709571500303, -23.78062553189673523, -0.9709657327914292813 ) ) ;
#84784=CARTESIAN_POINT ( 'NONE',  ( -0.07952141725841599396, -22.02053276243675128, 9.703205396196688426 ) ) ;
#84785=CARTESIAN_POINT ( 'NONE',  ( -7.839647760473957838, 19.78794240023834661, -1.500000000000002220 ) ) ;
#84786=CARTESIAN_POINT ( 'NONE',  ( -98.63223543337561239, -23.96169478059713853, 10.65365249895717881 ) ) ;
#84787=B_SPLINE_CURVE_WITH_KNOTS ( 'NONE', 3,
 ( #18375, #56458, #65580, #96495, #17373, #26991 ),
 .UNSPECIFIED., .F., .F.,
 ( 4, 2, 4 ),
 ( 1.570887131794638196E-05, 0.001396322306279761940, 0.002776935741241577573 ),
 .UNSPECIFIED. ) ;
#84789=B_SPLINE_CURVE_WITH_KNOTS ( 'NONE', 3,
 ( #17419, #71714, #2212, #33141 ),
 .UNSPECIFIED., .F., .F.,
 ( 4, 4 ),
 ( 0.000000000000000000, 9.999999999998897304E-05 ),
 .UNSPECIFIED. ) ;
#84790=CARTESIAN_POINT ( 'NONE',  ( -29.58953762381672092, -23.39424308723205570, 11.44779302747772221 ) ) ;
#84791=CARTESIAN_POINT ( 'NONE',  ( -29.62287095715005592, -23.40871900810292772, -1.443836166241315055 ) ) ;
#84793=CARTESIAN_POINT ( 'NONE',  ( 19.74966320730700176, -10.79507447929251107, -1.500000000000002220 ) ) ;
#84794=CARTESIAN_POINT ( 'NONE',  ( -108.8765244897739279, -25.30561928443788133, 5.929683345795315752 ) ) ;
#84795=ORIENTED_EDGE ( 'NONE', *, *, #26630, .F. ) ;
#84797=CARTESIAN_POINT ( 'NONE',  ( 5.117700956428186565, 18.95590836763280862, 11.49999999999999645 ) ) ;
#84799=CARTESIAN_POINT ( 'NONE',  ( -119.5228709571500474, -23.47593901973090524, -1.443836447538996204 ) ) ;
#84801=CARTESIAN_POINT ( 'NONE',  ( -88.58338171500136582, -24.66019654487199730, 8.947790411086115725 ) ) ;
#84802=CARTESIAN_POINT ( 'NONE',  ( -127.4728709571500360, -25.40558663563398767, 5.000950440326727531 ) ) ;
#84803=EDGE_CURVE ( 'NONE', #72503, #4570, #66501, .T. ) ;
#84804=CARTESIAN_POINT ( 'NONE',  ( -100.0218067620262303, -25.31439551943679689, 5.284572029636154689 ) ) ;
#84806=CARTESIAN_POINT ( 'NONE',  ( -9.297559507673007317, 17.40068379117045083, -1.500000000000002220 ) ) ;
#84807=ORIENTED_EDGE ( 'NONE', *, *, #78108, .T. ) ;
#84812=ORIENTED_EDGE ( 'NONE', *, *, #75756, .T. ) ;
#84813=CARTESIAN_POINT ( 'NONE',  ( -124.5228709571500758, -23.72773821059536914, 11.05748984161097326 ) ) ;
#84814=DIRECTION ( 'NONE',  ( 0.000000000000000000, 0.9999999999976377785, 2.173523156925979975E-06 ) ) ;
#84816=CARTESIAN_POINT ( 'NONE',  ( -98.89303308397303738, -25.26638225912975599, 6.110950151213043746 ) ) ;
#84817=CARTESIAN_POINT ( 'NONE',  ( -67.62287095715009855, -23.94994826722514958, -0.6494450866351695328 ) ) ;
#84818=CARTESIAN_POINT ( 'NONE',  ( -94.52287095715006160, -24.65952944569304961, 1.056160979905700570 ) ) ;
#84820=CARTESIAN_POINT ( 'NONE',  ( -61.52287095715006870, -23.96127896941632329, -0.6493128931038057994 ) ) ;
#84821=CARTESIAN_POINT ( 'NONE',  ( -18.23705311251027794, 8.147635122911419003, 11.49999999999998934 ) ) ;
#84822=EDGE_CURVE ( 'NONE', #53102, #68625, #46431, .T. ) ;
#84823=CARTESIAN_POINT ( 'NONE',  ( -45.52287095715007581, -23.47593901973090169, -1.443836447538997092 ) ) ;
#84824=CARTESIAN_POINT ( 'NONE',  ( -45.47439281453883808, -24.92592662359561118, 8.075495903018000021 ) ) ;
#84825=ORIENTED_EDGE ( 'NONE', *, *, #61879, .T. ) ;
#84826=B_SPLINE_CURVE_WITH_KNOTS ( 'NONE', 3,
 ( #31171, #62140, #23546, #49929, #40792, #18454 ),
 .UNSPECIFIED., .F., .F.,
 ( 4, 2, 4 ),
 ( 0.000000000000000000, 0.001380901958385392448, 0.002761803916770784895 ),
 .UNSPECIFIED. ) ;
#84828=B_SPLINE_CURVE_WITH_KNOTS ( 'NONE', 3,
 ( #16530, #319, #2336, #17546, #86558, #47506 ),
 .UNSPECIFIED., .F., .F.,
 ( 4, 2, 4 ),
 ( 6.384118678620252359E-06, 0.001386860460828383875, 0.002767336802978147530 ),
 .UNSPECIFIED. ) ;
#84829=CARTESIAN_POINT ( 'NONE',  ( -109.3592350823140720, -25.29012917042550512, 4.175497848340549822 ) ) ;
#84831=CARTESIAN_POINT ( 'NONE',  ( -120.6228709571500417, -24.63287334234178516, 0.9662140553045625024 ) ) ;
#84834=CARTESIAN_POINT ( 'NONE',  ( -119.6228709571500275, -24.33832256527049154, 0.1851278514138672837 ) ) ;
#84835=CARTESIAN_POINT ( 'NONE',  ( -83.55087393305831256, -24.15543982623907127, -0.2315651400026649820 ) ) ;
#84836=B_SPLINE_SURFACE_WITH_KNOTS ( 'NONE', 3, 3, ( 
 ( #83954, #91562, #52018, #66767 ),
 ( #13939, #68240, #74838, #97190 ),
 ( #5336, #51524, #97686, #90079 ),
 ( #29668, #89581, #20551, #98175 ),
 ( #12938, #20062, #43905, #59640 ),
 ( #21049, #98673, #44412, #22041 ),
 ( #5835, #29169, #60144, #45408 ) ),
 .UNSPECIFIED., .F., .F., .F.,
 ( 4, 3, 4 ),
 ( 4, 4 ),
 ( 0.7945040050992230318, 0.8970133687736492334, 0.9995227324480754350 ),
 ( 0.03950403576920281934, 0.04053499800853590379 ),
 .UNSPECIFIED. ) ;
#84837=CARTESIAN_POINT ( 'NONE',  ( -77.52287095715006160, -23.47596703998600631, 11.44779298504228571 ) ) ;
#84838=CARTESIAN_POINT ( 'NONE',  ( -40.52287095715005449, -24.99156044556202261, 7.747789690856173195 ) ) ;
#84840=CARTESIAN_POINT ( 'NONE',  ( -0.6865706486018943178, -20.24796467851281179, -1.500000000000002220 ) ) ;
#84841=CARTESIAN_POINT ( 'NONE',  ( -101.6228709571500559, -23.47593901973091235, -1.443836447539001089 ) ) ;
#84846=ORIENTED_EDGE ( 'NONE', *, *, #44736, .T. ) ;
#84847=DIRECTION ( 'NONE',  ( 0.000000000000000000, 0.9999999999976377785, 2.173523156925979975E-06 ) ) ;
#84848=CARTESIAN_POINT ( 'NONE',  ( 17.00595499256408871, 10.69956108467327205, -1.500000000000002220 ) ) ;
#84849=VECTOR ( 'NONE', #99325, 1000.000000000000114 ) ;
#84850=CARTESIAN_POINT ( 'NONE',  ( 10.44912437418449969, 18.32051524777507723, 11.49999999999999645 ) ) ;
#84852=CARTESIAN_POINT ( 'NONE',  ( -11.88820881604258339, -18.65297325734525913, -1.500000000000002220 ) ) ;
#84853=CARTESIAN_POINT ( 'NONE',  ( 20.52540449432101610, 0.9483640940595650104, 11.49999999999998934 ) ) ;
#84854=CARTESIAN_POINT ( 'NONE',  ( -95.60349032644573697, -23.48783264082477373, -1.443836473390088804 ) ) ;
#84855=CARTESIAN_POINT ( 'NONE',  ( -126.6228709571500275, -24.50216790748207529, 0.6166512839542536151 ) ) ;
#84856=ORIENTED_EDGE ( 'NONE', *, *, #96458, .T. ) ;
#84857=DIRECTION ( 'NONE',  ( 0.000000000000000000, -2.173523156925979552E-06, 0.9999999999976378895 ) ) ;
#84858=ORIENTED_EDGE ( 'NONE', *, *, #45630, .F. ) ;
#84859=CARTESIAN_POINT ( 'NONE',  ( -51.62287095715006302, -24.50216790748205753, 0.6166512839542510616 ) ) ;
#84860=CARTESIAN_POINT ( 'NONE',  ( -87.58953762381672448, -24.66019654487199730, 8.947790411086121054 ) ) ;
#84861=ORIENTED_EDGE ( 'NONE', *, *, #24368, .T. ) ;
#84862=EDGE_LOOP ( 'NONE', ( #54769, #72239, #92944, #17375 ) ) ;
#84863=ORIENTED_EDGE ( 'NONE', *, *, #28808, .T. ) ;
#84865=CARTESIAN_POINT ( 'NONE',  ( -31.52287095715006160, -23.47593901973090169, -1.443836447538997536 ) ) ;
#84867=CARTESIAN_POINT ( 'NONE',  ( -18.22997975830956108, -9.740667652671243459, -1.500000000000002220 ) ) ;
#84868=EDGE_CURVE ( 'NONE', #30829, #33008, #34407, .T. ) ;
#84869=CARTESIAN_POINT ( 'NONE',  ( 18.62697458635512859, 10.92912097662538251, 11.49999999999999645 ) ) ;
#84871=CARTESIAN_POINT ( 'NONE',  ( -83.62287095714999907, -24.33832256526968862, 0.1851278514119905905 ) ) ;
#84872=CARTESIAN_POINT ( 'NONE',  ( -60.62287095715006302, -24.62226745350437085, 0.9660975649728084091 ) ) ;
#84873=CARTESIAN_POINT ( 'NONE',  ( -8.633843874998758494, 20.65557450359631630, -1.500000000000002220 ) ) ;
#84874=CARTESIAN_POINT ( 'NONE',  ( -79.85862890617264043, -25.27875051067252699, 6.918725483278709731 ) ) ;
#84875=DIRECTION ( 'NONE',  ( 3.773278334444166432E-23, -1.000000000000000000, 0.000000000000000000 ) ) ;
#84876=ORIENTED_EDGE ( 'NONE', *, *, #73062, .T. ) ;
#84877=PLANE ( 'NONE',  #69549 ) ;
#84878=CARTESIAN_POINT ( 'NONE',  ( -49.58722086695681952, -24.35071581493542325, 9.817618358456035921 ) ) ;
#84880=CARTESIAN_POINT ( 'NONE',  ( -13.90609606471210391, -15.62508359690603221, 11.49999999999998934 ) ) ;
#84882=CARTESIAN_POINT ( 'NONE',  ( -86.55120064081188502, -24.15543982623907837, -0.2315651400026493834 ) ) ;
#84883=EDGE_LOOP ( 'NONE', ( #56564, #41490, #81017, #76790 ) ) ;
#84884=EDGE_CURVE ( 'NONE', #99016, #50353, #52248, .T. ) ;
#84885=CARTESIAN_POINT ( 'NONE',  ( -109.6235285740488479, -24.66019654487200441, 8.947790411086113949 ) ) ;
#84886=CARTESIAN_POINT ( 'NONE',  ( 21.17954554857512761, 0.9134790845329443520, -1.500000000000002220 ) ) ;
#84888=CARTESIAN_POINT ( 'NONE',  ( -93.62287095715005592, -29.50250243563736774, 8.947779886222139822 ) ) ;
#84890=CARTESIAN_POINT ( 'NONE',  ( -21.42251255223715134, 3.917230396363152067, -1.500000000000002220 ) ) ;
#84893=CARTESIAN_POINT ( 'NONE',  ( -35.52287095715006870, -24.99156044556120193, 7.747789690856173195 ) ) ;
#84894=CARTESIAN_POINT ( 'NONE',  ( -79.35269453762862213, -25.26523176223116351, 6.110756246060513597 ) ) ;
#84895=CARTESIAN_POINT ( 'NONE',  ( -0.06377455873143267340, 21.83884041771831619, -1.500000000000002220 ) ) ;
#84897=ORIENTED_EDGE ( 'NONE', *, *, #54068, .T. ) ;
#84899=DIRECTION ( 'NONE',  ( -3.773278334453079618E-23, 0.9999999999976377785, 2.173523156925979975E-06 ) ) ;
#84900=DIRECTION ( 'NONE',  ( 1.000000000000000000, 3.773278334444167608E-23, 8.201307833595939069E-29 ) ) ;
#84901=ORIENTED_EDGE ( 'NONE', *, *, #62600, .F. ) ;
#84902=EDGE_LOOP ( 'NONE', ( #65619, #83647, #60347, #98080 ) ) ;
#84905=CARTESIAN_POINT ( 'NONE',  ( 13.55612473118199723, -16.30799122071102403, 11.49999999999998934 ) ) ;
#84906=CARTESIAN_POINT ( 'NONE',  ( -94.62356957389862089, -24.65952944569304606, 1.056160979905703234 ) ) ;
#84907=CARTESIAN_POINT ( 'NONE',  ( -79.05725560372792415, -25.03138091265075715, 6.604864886565241733 ) ) ;
#84911=CARTESIAN_POINT ( 'NONE',  ( -13.40542139710017899, 13.98966777563825481, 11.49999999999998934 ) ) ;
#84912=CARTESIAN_POINT ( 'NONE',  ( -39.97884473287227536, -25.31392318313163159, 5.203682277190879724 ) ) ;
#84914=CARTESIAN_POINT ( 'NONE',  ( 19.29218144733592055, -2.436590042558338443, 11.49999999999999645 ) ) ;
#84915=DIRECTION ( 'NONE',  ( -3.773278334453080206E-23, 0.9999999999976377785, 2.173523156925979975E-06 ) ) ;
#84916=EDGE_CURVE ( 'NONE', #76505, #24959, #16169, .T. ) ;
#84922=LINE ( 'NONE', #15905, #46580 ) ;
#84924=FACE_OUTER_BOUND ( 'NONE', #40991, .T. ) ;
#84925=CARTESIAN_POINT ( 'NONE',  ( -34.52287095715006160, -23.48786465467240347, 11.44779295918255357 ) ) ;
#84926=CARTESIAN_POINT ( 'NONE',  ( 16.02095076306289201, 11.36058263404076030, 11.49999999999998934 ) ) ;
#84927=CARTESIAN_POINT ( 'NONE',  ( -41.46611000704998418, -25.31583576900412424, 4.188173601412459313 ) ) ;
#84928=ORIENTED_EDGE ( 'NONE', *, *, #4256, .F. ) ;
#84929=EDGE_CURVE ( 'NONE', #76612, #64842, #93695, .T. ) ;
#84930=CARTESIAN_POINT ( 'NONE',  ( -11.65619939812097527, 18.16556634249905855, 11.49999999999998934 ) ) ;
#84934=CARTESIAN_POINT ( 'NONE',  ( 20.16173082093541424, 11.17373015621797627, -1.500000000000002220 ) ) ;
#84936=CARTESIAN_POINT ( 'NONE',  ( -120.5228709571500616, -23.47593901973090524, -1.443836447538996204 ) ) ;
#84938=CARTESIAN_POINT ( 'NONE',  ( -121.5888783905858190, -24.51419770103157347, 9.386484678747175181 ) ) ;
#84939=CARTESIAN_POINT ( 'NONE',  ( -100.9084866940463883, -25.05508145465318748, 7.506936236879250934 ) ) ;
#84941=CARTESIAN_POINT ( 'NONE',  ( -129.5220747276651139, -23.96119346886880663, -0.6495511937831975890 ) ) ;
#84942=B_SPLINE_CURVE_WITH_KNOTS ( 'NONE', 3,
 ( #95600, #39808, #9861, #72276, #17473, #24577 ),
 .UNSPECIFIED., .F., .F.,
 ( 4, 2, 4 ),
 ( 6.391158118972359742E-06, 0.001387004593080793519, 0.002767618028042614572 ),
 .UNSPECIFIED. ) ;
#84943=CARTESIAN_POINT ( 'NONE',  ( -99.19491584893809488, -25.26400770206901214, 4.406300587698978255 ) ) ;
#84944=CARTESIAN_POINT ( 'NONE',  ( 4.300141163375406528, 19.41444791797076874, -1.500000000000002220 ) ) ;
#84945=ADVANCED_FACE ( 'NONE', ( #68962 ), #8567, .T. ) ;
#84947=CARTESIAN_POINT ( 'NONE',  ( -12.28770250403618114, -15.54288071925545722, -1.500000000000002220 ) ) ;
#84948=CARTESIAN_POINT ( 'NONE',  ( -56.63256988609624898, -24.34968618360933590, 0.1864209137778786995 ) ) ;
#84949=CARTESIAN_POINT ( 'NONE',  ( -39.22373867983765194, -25.29116667761266513, 3.518977199090397079 ) ) ;
#84951=CARTESIAN_POINT ( 'NONE',  ( 18.38559056850662543, 9.607341378227904016, 11.49999999999999645 ) ) ;
#84954=PLANE ( 'NONE',  #89508 ) ;
#84955=CARTESIAN_POINT ( 'NONE',  ( 16.28376985728763415, 15.88423345705086298, 11.49999999999999645 ) ) ;
#84956=VERTEX_POINT ( 'NONE', #15166 ) ;
#84959=CARTESIAN_POINT ( 'NONE',  ( -106.6228709571501128, -23.94994826722566117, -0.6494450866342750261 ) ) ;
#84960=CARTESIAN_POINT ( 'NONE',  ( 20.15506735835773000, -1.303320585059813741, 11.49999999999998934 ) ) ;
#84961=FACE_OUTER_BOUND ( 'NONE', #84883, .T. ) ;
#84963=CARTESIAN_POINT ( 'NONE',  ( -52.52287095715006160, -24.50321055353804311, 9.387540953477529371 ) ) ;
#84965=EDGE_CURVE ( 'NONE', #100338, #14117, #2971, .T. ) ;
#84966=EDGE_LOOP ( 'NONE', ( #93451, #95127, #12247, #56615 ) ) ;
#84968=CARTESIAN_POINT ( 'NONE',  ( -12.24191887126339751, 19.33842681661653984, -1.500000000000002220 ) ) ;
#84969=CARTESIAN_POINT ( 'NONE',  ( -51.28182533633388829, -25.27420685139605894, 3.855515792242854012 ) ) ;
#84970=EDGE_CURVE ( 'NONE', #58107, #11670, #52554, .T. ) ;
#84971=CARTESIAN_POINT ( 'NONE',  ( -21.09935167195790839, -4.734744157926700225, -1.500000000000002220 ) ) ;
#84972=FACE_OUTER_BOUND ( 'NONE', #40717, .T. ) ;
#84973=FACE_OUTER_BOUND ( 'NONE', #10150, .T. ) ;
#84974=CARTESIAN_POINT ( 'NONE',  ( -7.049398010371669798, 19.71092172866906012, 11.49999999999999645 ) ) ;
#84975=VERTEX_POINT ( 'NONE', #23780 ) ;
#84976=CARTESIAN_POINT ( 'NONE',  ( -124.5211395258430400, -23.96119346886880663, -0.6495511937832024740 ) ) ;
#84977=CARTESIAN_POINT ( 'NONE',  ( -21.99024891984110752, 1.279939690139831665, 11.49999999999998934 ) ) ;
#84979=CARTESIAN_POINT ( 'NONE',  ( -105.6382438712245460, -23.48786465467241769, 11.44779295918254114 ) ) ;
#84980=CARTESIAN_POINT ( 'NONE',  ( -30.47287095715008576, -24.38457522042859438, 9.689408350323725827 ) ) ;
#84981=VERTEX_POINT ( 'NONE', #54252 ) ;
#84983=DIRECTION ( 'NONE',  ( -0.000000000000000000, 2.173523156925979552E-06, -0.9999999999976378895 ) ) ;
#84988=CARTESIAN_POINT ( 'NONE',  ( -71.54955542377307154, -24.15620529776628445, 10.23563542870660115 ) ) ;
#84989=CARTESIAN_POINT ( 'NONE',  ( -101.7667076177128678, -25.10936043410780982, 3.940952065299377249 ) ) ;
#84991=CARTESIAN_POINT ( 'NONE',  ( -12.74120943341865342, -16.01528480738631899, -1.500000000000002220 ) ) ;
#84994=CARTESIAN_POINT ( 'NONE',  ( -110.5895376238167387, -24.99156044556202971, 7.747789690856174083 ) ) ;
#84995=CARTESIAN_POINT ( 'NONE',  ( -44.56061633354861584, -23.73766607897669800, -1.055555164236459120 ) ) ;
#84997=CARTESIAN_POINT ( 'NONE',  ( 17.40631026334068565, 13.93540124644318645, 11.49999999999998934 ) ) ;
#84999=CARTESIAN_POINT ( 'NONE',  ( -91.52287095715006160, -24.33832256527048088, 0.1851278514138647024 ) ) ;
#85000=VERTEX_POINT ( 'NONE', #40012 ) ;
#85002=CARTESIAN_POINT ( 'NONE',  ( -39.52287095715006870, -23.48786465467241058, 11.44779295918255180 ) ) ;
#85003=CARTESIAN_POINT ( 'NONE',  ( -14.80784184970232431, -14.63167926507950689, -1.500000000000002220 ) ) ;
#85004=VERTEX_POINT ( 'NONE', #77556 ) ;
#85007=CARTESIAN_POINT ( 'NONE',  ( -98.52287095715009002, -24.51387760970724727, 9.387446482453409402 ) ) ;
#85008=ORIENTED_EDGE ( 'NONE', *, *, #14916, .T. ) ;
#85009=ORIENTED_EDGE ( 'NONE', *, *, #71038, .F. ) ;
#85010=CARTESIAN_POINT ( 'NONE',  ( -31.62287095715005236, -29.50248528299804818, 1.056150453629029817 ) ) ;
#85011=CARTESIAN_POINT ( 'NONE',  ( -121.5895376238167245, -23.48786465467241769, 11.44779295918253759 ) ) ;
#85013=LINE ( 'NONE', #30736, #4808 ) ;
#85014=CARTESIAN_POINT ( 'NONE',  ( -92.63718633548049297, -23.73791477778911840, 11.05961554403170588 ) ) ;
#85015=PLANE ( 'NONE',  #90206 ) ;
#85016=CARTESIAN_POINT ( 'NONE',  ( 0.7529269182969693386, -22.20201975079678647, 11.49999999999999645 ) ) ;
#85018=CARTESIAN_POINT ( 'NONE',  ( -105.5562042904834215, -23.47596703998600631, 11.44779298504227683 ) ) ;
#85020=CARTESIAN_POINT ( 'NONE',  ( 21.71957326813621592, -6.446789169762093152, -1.500000000000002220 ) ) ;
#85021=B_SPLINE_CURVE_WITH_KNOTS ( 'NONE', 3,
 ( #86512, #16996, #47963, #88522 ),
 .UNSPECIFIED., .F., .F.,
 ( 4, 4 ),
 ( 0.7303074191294323114, 0.7393138504015477341 ),
 .UNSPECIFIED. ) ;
#85022=CARTESIAN_POINT ( 'NONE',  ( -115.5567998953322046, -23.85049219812686871, 10.88485053497526778 ) ) ;
#85023=ORIENTED_EDGE ( 'NONE', *, *, #81295, .F. ) ;
#85028=CARTESIAN_POINT ( 'NONE',  ( -14.78635263257777233, 13.65558988533819473, 11.49999999999998934 ) ) ;
#85029=B_SPLINE_SURFACE_WITH_KNOTS ( 'NONE', 3, 3, ( 
 ( #16181, #54263, #8072, #39019 ),
 ( #93297, #55266, #39527, #31916 ),
 ( #93807, #24300, #86198, #16681 ),
 ( #1976, #26799, #79584, #19175 ),
 ( #32919, #81087, #10074, #57762 ),
 ( #88208, #26302, #9573, #27301 ),
 ( #10569, #87198, #11563, #40538 ) ),
 .UNSPECIFIED., .F., .F., .F.,
 ( 4, 3, 4 ),
 ( 4, 4 ),
 ( 0.7945040050992245861, 0.8970133687736504546, 0.9995227324480763231 ),
 ( 0.7396819606801936509, 0.7410361715128946924 ),
 .UNSPECIFIED. ) ;
#85031=VERTEX_POINT ( 'NONE', #38012 ) ;
#85032=CARTESIAN_POINT ( 'NONE',  ( -89.81226385320383088, -25.26364009184147008, 3.993462176398974162 ) ) ;
#85033=CARTESIAN_POINT ( 'NONE',  ( 18.00092565640838416, -13.26076702590692769, -1.500000000000002220 ) ) ;
#85035=ORIENTED_EDGE ( 'NONE', *, *, #79352, .T. ) ;
#85039=ADVANCED_FACE ( 'NONE', ( #22765 ), #45318, .T. ) ;
#85040=ADVANCED_FACE ( 'NONE', ( #19163 ), #42531, .T. ) ;
#85042=ADVANCED_FACE ( 'NONE', ( #1965 ), #6422, .T. ) ;
#85043=FACE_BOUND ( 'NONE', #8003, .T. ) ;
#85044=CARTESIAN_POINT ( 'NONE',  ( -5.499840656826012975, 18.73951620154120334, -1.500000000000002220 ) ) ;
#85047=CARTESIAN_POINT ( 'NONE',  ( 19.19993882694861753, 9.668096177433461946, 11.49999999999998934 ) ) ;
#85048=CARTESIAN_POINT ( 'NONE',  ( -36.52287095715006870, -23.73907113216988307, -1.053371485793256124 ) ) ;
#85050=CARTESIAN_POINT ( 'NONE',  ( -71.58953762381672448, -23.48786465467241413, 11.44779295918254469 ) ) ;
#85052=CARTESIAN_POINT ( 'NONE',  ( 19.82229641098322404, 11.46754112681587046, -1.500000000000002220 ) ) ;
#85055=CARTESIAN_POINT ( 'NONE',  ( -85.52287095715006160, -23.47596703998600631, 11.44779298504228393 ) ) ;
#85056=CARTESIAN_POINT ( 'NONE',  ( -51.52764846858840997, -25.25773520710183817, 6.187572766161611781 ) ) ;
#85057=CARTESIAN_POINT ( 'NONE',  ( -6.237196068801617699, -19.06703463882530158, 11.49999999999999645 ) ) ;
#85058=CARTESIAN_POINT ( 'NONE',  ( -80.21014334459538020, -25.26612374374091630, 4.508707588862841398 ) ) ;
#85059=DIRECTION ( 'NONE',  ( -3.773278334453079618E-23, 0.9999999999976377785, 2.173523156925978705E-06 ) ) ;
#85061=FACE_OUTER_BOUND ( 'NONE', #54407, .T. ) ;
#85063=CARTESIAN_POINT ( 'NONE',  ( -109.5228709571500758, -23.72747288104470798, -1.053458166803225682 ) ) ;
#85064=ADVANCED_FACE ( 'NONE', ( #19660 ), #20960, .T. ) ;
#85066=VECTOR ( 'NONE', #79636, 1000.000000000000114 ) ;
#85067=CARTESIAN_POINT ( 'NONE',  ( -21.04499429308205549, 5.405531755741471045, -1.500000000000002220 ) ) ;
#85069=CARTESIAN_POINT ( 'NONE',  ( -19.57149217635686966, 1.386223266712492297, -1.500000000000002220 ) ) ;
#85070=VECTOR ( 'NONE', #56689, 1000.000000000000114 ) ;
#85071=CARTESIAN_POINT ( 'NONE',  ( -128.5562042904833788, -24.64898659630529565, 1.056161002820832806 ) ) ;
#85072=EDGE_CURVE ( 'NONE', #76499, #27790, #21157, .T. ) ;
#85073=CARTESIAN_POINT ( 'NONE',  ( -109.6235167689328591, -25.31698100855897593, 4.923693415162312625 ) ) ;
#85075=DIRECTION ( 'NONE',  ( -3.773278334444166432E-23, 1.000000000000000000, 0.000000000000000000 ) ) ;
#85077=CARTESIAN_POINT ( 'NONE',  ( -18.72588118538106272, -8.511115862834014223, 11.49999999999999645 ) ) ;
#85078=CARTESIAN_POINT ( 'NONE',  ( -39.07219716201183246, -25.30584882308033912, 4.512390342206024307 ) ) ;
#85079=EDGE_CURVE ( 'NONE', #44226, #50353, #54890, .T. ) ;
#85083=CARTESIAN_POINT ( 'NONE',  ( -46.62287095715006302, -23.96127896941632685, -0.6493128931037863705 ) ) ;
#85084=CARTESIAN_POINT ( 'NONE',  ( -39.98073487448829155, -25.28892444151557939, 3.395433753900389373 ) ) ;
#85085=CARTESIAN_POINT ( 'NONE',  ( -125.5196039661687877, -24.83644354573579349, 8.397322867130096569 ) ) ;
#85086=CARTESIAN_POINT ( 'NONE',  ( -121.6228709571500417, -24.64965695001469115, 8.947790433994175174 ) ) ;
#85087=PLANE ( 'NONE',  #12759 ) ;
#85088=CARTESIAN_POINT ( 'NONE',  ( -124.6228709571501412, -24.35013146730204525, 9.818937971375104823 ) ) ;
#85089=EDGE_CURVE ( 'NONE', #10184, #17176, #75939, .T. ) ;
#85090=CARTESIAN_POINT ( 'NONE',  ( -21.10450430117995424, 9.351148110661185342, 11.49999999999999645 ) ) ;
#85091=CARTESIAN_POINT ( 'NONE',  ( 22.73759373355791169, -1.750760473330008171, 11.49999999999998934 ) ) ;
#85093=CARTESIAN_POINT ( 'NONE',  ( -67.52287095715004739, -24.51283580621365132, 0.6167428607019708187 ) ) ;
#85094=CARTESIAN_POINT ( 'NONE',  ( -85.62287095715004170, -24.99156045073393173, 7.747789690856161648 ) ) ;
#85096=CARTESIAN_POINT ( 'NONE',  ( -22.05133119090760019, 4.102169094691678453, 11.49999999999999645 ) ) ;
#85098=B_SPLINE_CURVE_WITH_KNOTS ( 'NONE', 3,
 ( #51935, #89990, #5748, #12852, #67172, #59551, #97105, #50941 ),
 .UNSPECIFIED., .F., .F.,
 ( 4, 2, 2, 4 ),
 ( 6.384118678604512793E-06, 0.002007151183507257554, 0.003007534715921582509, 0.004007918248335906597 ),
 .UNSPECIFIED. ) ;
#85099=LINE ( 'NONE', #85597, #31409 ) ;
#85100=CARTESIAN_POINT ( 'NONE',  ( -38.62287095715004881, -24.50321055353804311, 9.387540953477525818 ) ) ;
#85101=ADVANCED_FACE ( 'NONE', ( #27783 ), #29777, .T. ) ;
#85102=CARTESIAN_POINT ( 'NONE',  ( 9.922928194174257754, 19.57116106031148561, 11.49999999999998934 ) ) ;
#85104=CARTESIAN_POINT ( 'NONE',  ( -87.63200167382973405, -24.15620529776628445, 10.23563542870660292 ) ) ;
#85105=CARTESIAN_POINT ( 'NONE',  ( -38.62287095715005592, -29.50250786944525672, 11.44777988621624232 ) ) ;
#85106=LINE ( 'NONE', #77482, #33014 ) ;
#85108=VERTEX_POINT ( 'NONE', #20162 ) ;
#85109=CARTESIAN_POINT ( 'NONE',  ( 5.889875310795558150, 19.62242631308348706, 11.49999999999998934 ) ) ;
#85110=VERTEX_POINT ( 'NONE', #51124 ) ;
#85112=EDGE_LOOP ( 'NONE', ( #40361, #12724, #35612, #39443 ) ) ;
#85114=CARTESIAN_POINT ( 'NONE',  ( 7.103900956763240515, -21.94381868531750968, -1.500000000000002220 ) ) ;
#85116=CARTESIAN_POINT ( 'NONE',  ( 14.62039552936377085, -14.08751720214925207, -1.500000000000002220 ) ) ;
#85117=VERTEX_POINT ( 'NONE', #74455 ) ;
#85118=CARTESIAN_POINT ( 'NONE',  ( -27.14006706031606697, -25.03993259027813778, 4.938174481708933250 ) ) ;
#85120=B_SPLINE_CURVE_WITH_KNOTS ( 'NONE', 3,
 ( #48993, #41374, #72326, #89543, #50992, #4810 ),
 .UNSPECIFIED., .F., .F.,
 ( 4, 2, 4 ),
 ( 0.000000000000000000, 0.001380901958385390930, 0.002761803916770781860 ),
 .UNSPECIFIED. ) ;
#85121=CARTESIAN_POINT ( 'NONE',  ( -28.52287095715006160, -23.56429130584908194, 11.05761041701457792 ) ) ;
#85122=CARTESIAN_POINT ( 'NONE',  ( -70.62753759711341672, -24.83618233451450052, 1.606449574219541487 ) ) ;
#85123=CARTESIAN_POINT ( 'NONE',  ( 20.53733210929814845, -6.371126427052321795, 11.49999999999999645 ) ) ;
#85125=CARTESIAN_POINT ( 'NONE',  ( -75.58253337940892891, -24.83618233451450763, 1.606449574219540599 ) ) ;
#85126=CARTESIAN_POINT ( 'NONE',  ( -61.62756372973229446, -24.51419770103157347, 9.386484678747178734 ) ) ;
#85128=CARTESIAN_POINT ( 'NONE',  ( 20.29938135082171158, -4.300543036493735372, 11.49999999999998934 ) ) ;
#85132=ORIENTED_EDGE ( 'NONE', *, *, #24438, .F. ) ;
#85133=CARTESIAN_POINT ( 'NONE',  ( -111.5539194383848098, -24.15620529776629510, 10.23563542870659582 ) ) ;
#85134=DIRECTION ( 'NONE',  ( 1.000000000000000000, 3.773278334444167608E-23, 8.201307833595939069E-29 ) ) ;
#85138=CARTESIAN_POINT ( 'NONE',  ( -111.6228709571500559, -29.50248528299804818, 1.056150453629043584 ) ) ;
#85139=CARTESIAN_POINT ( 'NONE',  ( -65.62561733370567651, -24.92564183028979130, 1.928384488918254869 ) ) ;
#85140=CARTESIAN_POINT ( 'NONE',  ( 17.71009474140864981, 13.04663522181963309, 11.49999999999999645 ) ) ;
#85143=CARTESIAN_POINT ( 'NONE',  ( -3.649967738973055376, -22.27025559232234642, -1.500000000000002220 ) ) ;
#85145=CARTESIAN_POINT ( 'NONE',  ( -20.70934228997045068, 3.328930095467914185, -1.500000000000002220 ) ) ;
#85149=CARTESIAN_POINT ( 'NONE',  ( -80.62287095715002749, -24.51163499207174112, 0.6490370598554275894 ) ) ;
#85151=CARTESIAN_POINT ( 'NONE',  ( -18.46100929034391314, -11.06139713797464985, -1.500000000000002220 ) ) ;
#85153=ORIENTED_EDGE ( 'NONE', *, *, #63658, .T. ) ;
#85154=CARTESIAN_POINT ( 'NONE',  ( -5.075574613727041218, 20.51645923614106337, -1.500000000000002220 ) ) ;
#85155=DIRECTION ( 'NONE',  ( -3.773278334453079030E-23, 0.9999999999976377785, 2.173523156925979128E-06 ) ) ;
#85157=CARTESIAN_POINT ( 'NONE',  ( -61.66031320541097216, -25.33009847151395633, 4.495758292450051208 ) ) ;
#85158=CARTESIAN_POINT ( 'NONE',  ( -121.5537572759010061, -24.51314013834315375, 0.6176544820404190617 ) ) ;
#85160=CARTESIAN_POINT ( 'NONE',  ( -117.6228709571500559, -24.64898659630368627, 1.056161002820833028 ) ) ;
#85161=CARTESIAN_POINT ( 'NONE',  ( -22.11188964843745453, -1.696007508606716341, -1.500000000000002220 ) ) ;
#85165=ORIENTED_EDGE ( 'NONE', *, *, #81187, .T. ) ;
#85167=CARTESIAN_POINT ( 'NONE',  ( -37.66608410079602010, -23.48783264082478084, -1.443836473390075703 ) ) ;
#85168=CARTESIAN_POINT ( 'NONE',  ( -40.49165087243459737, -25.30353303947430987, 5.543942858925161588 ) ) ;
#85169=ADVANCED_FACE ( 'NONE', ( #52125 ), #12030, .T. ) ;
#85172=CARTESIAN_POINT ( 'NONE',  ( -14.69715086760845857, -12.76062437926726290, 11.49999999999998934 ) ) ;
#85174=CARTESIAN_POINT ( 'NONE',  ( -6.079122355442096115, 20.50309271558274915, -1.500000000000002220 ) ) ;
#85175=CARTESIAN_POINT ( 'NONE',  ( -62.55964909848019317, -23.73766607897669445, -1.055555164236454901 ) ) ;
#85177=CARTESIAN_POINT ( 'NONE',  ( -106.6228709571500559, -24.65952944569304606, 1.056160979905703012 ) ) ;
#85178=CARTESIAN_POINT ( 'NONE',  ( -109.8650282762807393, -25.28040082146351608, 5.784628005357986602 ) ) ;
#85179=B_SPLINE_CURVE_WITH_KNOTS ( 'NONE', 3,
 ( #78527, #924, #46606, #55727, #77031, #69929 ),
 .UNSPECIFIED., .F., .F.,
 ( 4, 2, 4 ),
 ( 0.000000000000000000, 0.001380901958385383124, 0.002761803916770766247 ),
 .UNSPECIFIED. ) ;
#85180=CARTESIAN_POINT ( 'NONE',  ( -7.311831771877058905, -21.45741656709679646, -1.500000000000002220 ) ) ;
#85182=DIRECTION ( 'NONE',  ( 3.773278334444167608E-23, -1.000000000000000000, 0.000000000000000000 ) ) ;
#85183=CARTESIAN_POINT ( 'NONE',  ( -127.6228709571500559, -24.34917612406838572, 0.1852690917426747241 ) ) ;
#85184=CARTESIAN_POINT ( 'NONE',  ( 2.793900936927258272, 19.68708943014846469, 11.49999999999999645 ) ) ;
#85185=CARTESIAN_POINT ( 'NONE',  ( -69.52287095715011844, -23.73907113216989018, -1.053371485793251239 ) ) ;
#85186=CARTESIAN_POINT ( 'NONE',  ( -73.62287095715004170, -24.50216790748098461, 0.6166512839513668132 ) ) ;
#85187=EDGE_LOOP ( 'NONE', ( #12119, #86657, #1996, #1413 ) ) ;
#85188=CARTESIAN_POINT ( 'NONE',  ( -60.52287095715004028, -24.92579138211018730, 1.929029949965656909 ) ) ;
#85189=DIRECTION ( 'NONE',  ( -0.000000000000000000, 2.173523156925979552E-06, -0.9999999999976378895 ) ) ;
#85190=CARTESIAN_POINT ( 'NONE',  ( -68.52287095715009002, -24.51283580621364422, 0.6167428607019779241 ) ) ;
#85191=CARTESIAN_POINT ( 'NONE',  ( 16.53012286974688294, -13.99140274789385252, 11.49999999999998934 ) ) ;
#85192=CARTESIAN_POINT ( 'NONE',  ( -124.6228709571500559, -24.64898659630368627, 1.056161002820833028 ) ) ;
#85193=CARTESIAN_POINT ( 'NONE',  ( 15.33136405852079243, -11.96835230219363311, -1.500000000000002220 ) ) ;
#85195=DIRECTION ( 'NONE',  ( -3.773278334453080206E-23, 0.9999999999976377785, 2.173523156925979975E-06 ) ) ;
#85196=CARTESIAN_POINT ( 'NONE',  ( 19.41305359857673096, 4.112862643401165919, 11.49999999999998934 ) ) ;
#85197=ORIENTED_EDGE ( 'NONE', *, *, #41552, .T. ) ;
#85198=CARTESIAN_POINT ( 'NONE',  ( 18.82434097252966154, -7.598309640217090433, 11.49999999999999645 ) ) ;
#85199=LINE ( 'NONE', #38029, #24547 ) ;
#85202=EDGE_LOOP ( 'NONE', ( #22729, #93005, #93142, #66064 ) ) ;
#85203=DIRECTION ( 'NONE',  ( -3.773278334453079030E-23, 0.9999999999976377785, 2.173523156925978705E-06 ) ) ;
#85204=CARTESIAN_POINT ( 'NONE',  ( -114.5228709571500616, -29.50248528299804818, 1.056150453629043584 ) ) ;
#85205=CARTESIAN_POINT ( 'NONE',  ( -49.63502199369077772, -25.31601829474233156, 4.997541875046982440 ) ) ;
#85207=CARTESIAN_POINT ( 'NONE',  ( -40.62513804936914852, -23.48786465467240347, 11.44779295918255180 ) ) ;
#85209=CARTESIAN_POINT ( 'NONE',  ( -59.62287095715004881, -29.50250786944525672, 11.44777988621623876 ) ) ;
#85210=CARTESIAN_POINT ( 'NONE',  ( 16.71511084712224360, -11.16500066668146829, -1.500000000000002220 ) ) ;
#85211=VECTOR ( 'NONE', #17920, 1000.000000000000114 ) ;
#85212=CARTESIAN_POINT ( 'NONE',  ( -89.52287095715009002, -24.66019654487200441, 8.947790411086119278 ) ) ;
#85213=EDGE_LOOP ( 'NONE', ( #13596, #46579, #82581, #67406 ) ) ;
#85216=ADVANCED_FACE ( 'NONE', ( #61246 ), #15041, .F. ) ;
#85217=CARTESIAN_POINT ( 'NONE',  ( 21.75204538223844963, -7.182240389990739438, 11.49999999999999645 ) ) ;
#85218=CARTESIAN_POINT ( 'NONE',  ( -0.6305239314742796530, -22.70799625201654592, -1.500000000000002220 ) ) ;
#85219=VERTEX_POINT ( 'NONE', #31778 ) ;
#85221=CARTESIAN_POINT ( 'NONE',  ( -126.5228709571500900, -24.35013146730205236, 9.818937971375095941 ) ) ;
#85222=DIRECTION ( 'NONE',  ( -3.773278334453079618E-23, 0.9999999999976377785, 2.173523156925979975E-06 ) ) ;
#85223=CARTESIAN_POINT ( 'NONE',  ( -36.52287095715006870, -29.50250243563736774, 8.947779886222148704 ) ) ;
#85225=CARTESIAN_POINT ( 'NONE',  ( -128.5896661346126564, -24.35071581493544102, 9.817618358456018157 ) ) ;
#85227=ORIENTED_EDGE ( 'NONE', *, *, #93457, .F. ) ;
#85228=CARTESIAN_POINT ( 'NONE',  ( -6.692510123977180925, 19.25193956699996178, 11.49999999999998934 ) ) ;
#85229=ORIENTED_EDGE ( 'NONE', *, *, #12659, .F. ) ;
#85230=CARTESIAN_POINT ( 'NONE',  ( -22.87025945403008365, 2.249016246415321163, 11.49999999999998934 ) ) ;
#85231=CARTESIAN_POINT ( 'NONE',  ( -54.56007923198101395, -23.73791477778911485, 11.05961554403171121 ) ) ;
#85234=CARTESIAN_POINT ( 'NONE',  ( -81.46833269854555226, -25.24078552941144693, 6.350783917184607219 ) ) ;
#85236=CARTESIAN_POINT ( 'NONE',  ( -4.607724273132460802, 20.83226218841027944, 11.49999999999999645 ) ) ;
#85237=VERTEX_POINT ( 'NONE', #68844 ) ;
#85239=CARTESIAN_POINT ( 'NONE',  ( 4.265775719338400052, 21.77767432286298543, -1.500000000000002220 ) ) ;
#85240=CARTESIAN_POINT ( 'NONE',  ( -1.706377481887368486, -20.59057665607738130, 11.49999999999998934 ) ) ;
#85241=ORIENTED_EDGE ( 'NONE', *, *, #40753, .F. ) ;
#85243=FACE_OUTER_BOUND ( 'NONE', #91878, .T. ) ;
#85247=ORIENTED_EDGE ( 'NONE', *, *, #63336, .F. ) ;
#85248=CARTESIAN_POINT ( 'NONE',  ( -56.55620429048339304, -24.64965694238574301, 8.947790433994201820 ) ) ;
#85249=DIRECTION ( 'NONE',  ( -3.773278334453079030E-23, 0.9999999999976377785, 2.173523156925979128E-06 ) ) ;
#85250=CARTESIAN_POINT ( 'NONE',  ( 7.312689604342500260, -19.48077458720139532, -1.500000000000002220 ) ) ;
#85251=CARTESIAN_POINT ( 'NONE',  ( 20.57308398666954119, -7.222494929537193187, 11.49999999999999645 ) ) ;
#85254=CARTESIAN_POINT ( 'NONE',  ( -78.56385301586374226, -23.48786465467241058, 11.44779295918254469 ) ) ;
#85255=CARTESIAN_POINT ( 'NONE',  ( -19.72384299526936857, -10.77339039931002773, -1.500000000000002220 ) ) ;
#85256=AXIS2_PLACEMENT_3D ( 'NONE', #61375, #32415, #76565 ) ;
#85257=CARTESIAN_POINT ( 'NONE',  ( -38.60881210526748220, -23.73766607897670511, -1.055555164236442689 ) ) ;
#85261=ORIENTED_EDGE ( 'NONE', *, *, #13103, .F. ) ;
#85262=ORIENTED_EDGE ( 'NONE', *, *, #80510, .F. ) ;
#85264=CARTESIAN_POINT ( 'NONE',  ( -9.778911232092227124, -18.99720643767551209, -1.500000000000002220 ) ) ;
#85265=VERTEX_POINT ( 'NONE', #7430 ) ;
#85267=CARTESIAN_POINT ( 'NONE',  ( -15.31302551872622075, -14.39686070098267479, -1.500000000000002220 ) ) ;
#85268=CARTESIAN_POINT ( 'NONE',  ( -30.61626898804283670, -24.27850102686685929, 0.04395666736089842014 ) ) ;
#85269=EDGE_CURVE ( 'NONE', #20866, #65831, #63352, .T. ) ;
#85270=CARTESIAN_POINT ( 'NONE',  ( -99.56303788721014314, -25.24522941805722098, 3.791487066088053748 ) ) ;
#85271=VECTOR ( 'NONE', #68926, 1000.000000000000114 ) ;
#85273=CARTESIAN_POINT ( 'NONE',  ( -6.887433846447126307, -20.85920400149894149, -1.500000000000002220 ) ) ;
#85278=ADVANCED_FACE ( 'NONE', ( #24158 ), #47008, .T. ) ;
#85280=CARTESIAN_POINT ( 'NONE',  ( -19.40664508603899563, 7.695215611089875729, 11.49999999999999645 ) ) ;
#85281=AXIS2_PLACEMENT_3D ( 'NONE', #40555, #50659, #42561 ) ;
#85282=EDGE_CURVE ( 'NONE', #57581, #58432, #41597, .T. ) ;
#85284=EDGE_CURVE ( 'NONE', #14950, #11637, #70698, .T. ) ;
#85285=CARTESIAN_POINT ( 'NONE',  ( -125.5228709571500616, -24.99156044556120904, 7.747789690856173195 ) ) ;
#85286=CARTESIAN_POINT ( 'NONE',  ( -10.19904512095640037, -23.73149035699961473, 5.002395802403317049 ) ) ;
#85287=CARTESIAN_POINT ( 'NONE',  ( -3.120219904758775975, 21.05623772282662998, -1.500000000000002220 ) ) ;
#85288=CARTESIAN_POINT ( 'NONE',  ( -104.5228709571500758, -23.48786465467241769, 11.44779295918254114 ) ) ;
#85289=ADVANCED_FACE ( 'NONE', ( #32275 ), #70847, .F. ) ;
#85290=CARTESIAN_POINT ( 'NONE',  ( -107.6248333959935053, -24.51419770103157703, 9.386484678747169852 ) ) ;
#85291=CARTESIAN_POINT ( 'NONE',  ( -122.5228709571500616, -24.65952944569305316, 1.056160979905705899 ) ) ;
#85293=CARTESIAN_POINT ( 'NONE',  ( -18.84819291449097278, 12.34854029719970825, -1.500000000000002220 ) ) ;
#85294=CARTESIAN_POINT ( 'NONE',  ( -118.6228709571500701, -23.48786465467241769, 11.44779295918253759 ) ) ;
#85297=CARTESIAN_POINT ( 'NONE',  ( -19.44079195400435012, 3.002763184081948200, 11.49999999999999645 ) ) ;
#85301=VERTEX_POINT ( 'NONE', #46504 ) ;
#85302=CARTESIAN_POINT ( 'NONE',  ( -89.52287095715007581, -23.72773821059536203, 11.05748984161097326 ) ) ;
#85303=LINE ( 'NONE', #6680, #1043 ) ;
#85304=CARTESIAN_POINT ( 'NONE',  ( -99.94284412489217573, -25.25095800927872958, 5.308582836096728208 ) ) ;
#85305=VECTOR ( 'NONE', #6001, 1000.000000000000114 ) ;
#85306=CARTESIAN_POINT ( 'NONE',  ( 2.412641546452875208, 19.58572291230954221, -1.500000000000002220 ) ) ;
#85311=FACE_OUTER_BOUND ( 'NONE', #34093, .T. ) ;
#85312=FACE_OUTER_BOUND ( 'NONE', #22815, .T. ) ;
#85313=CARTESIAN_POINT ( 'NONE',  ( -55.57730862517797732, -24.92564183028978775, 1.928384488918253092 ) ) ;
#85314=LINE ( 'NONE', #7698, #31461 ) ;
#85315=PLANE ( 'NONE',  #79271 ) ;
#85317=CARTESIAN_POINT ( 'NONE',  ( -113.6228709571500559, -29.50250243563736774, 8.947779886222136270 ) ) ;
#85318=CARTESIAN_POINT ( 'NONE',  ( 10.17626895549074817, -17.22257424524772418, -1.500000000000002220 ) ) ;
#85319=EDGE_CURVE ( 'NONE', #100298, #96024, #29530, .T. ) ;
#85320=DIRECTION ( 'NONE',  ( 0.000000000000000000, 0.9999999999976377785, 2.173523156925979128E-06 ) ) ;
#85321=CARTESIAN_POINT ( 'NONE',  ( -45.64357623215011728, -24.40133493613049964, 9.663955038902802386 ) ) ;
#85322=ORIENTED_EDGE ( 'NONE', *, *, #23881, .F. ) ;
#85323=AXIS2_PLACEMENT_3D ( 'NONE', #13175, #98410, #59882 ) ;
#85324=ADVANCED_FACE ( 'NONE', ( #54130 ), #95681, .F. ) ;
#85326=CARTESIAN_POINT ( 'NONE',  ( -109.3965479632025080, -25.29012866004314830, 3.940679847089471277 ) ) ;
#85327=CARTESIAN_POINT ( 'NONE',  ( -58.52287095715006870, -23.96177878511308990, 10.65340807706330217 ) ) ;
#85328=CARTESIAN_POINT ( 'NONE',  ( -106.5562042904833930, -23.48786465467241769, 11.44779295918252870 ) ) ;
#85329=CARTESIAN_POINT ( 'NONE',  ( -119.2834313257731935, -25.38352531986205207, 4.245363004327347589 ) ) ;
#85330=CARTESIAN_POINT ( 'NONE',  ( -83.59183548183668222, -24.15543982623906771, -0.2315651400026649265 ) ) ;
#85332=FACE_OUTER_BOUND ( 'NONE', #34095, .T. ) ;
#85333=EDGE_CURVE ( 'NONE', #43203, #71288, #73048, .T. ) ;
#85334=CARTESIAN_POINT ( 'NONE',  ( -40.52287095715007581, -24.82576562948890597, 8.398263436605414967 ) ) ;
#85338=CARTESIAN_POINT ( 'NONE',  ( 11.01437679584920026, 17.03896688766576517, -1.500000000000002220 ) ) ;
#85342=DIRECTION ( 'NONE',  ( 0.000000000000000000, 2.173523156925980399E-06, -0.9999999999976378895 ) ) ;
#85343=EDGE_LOOP ( 'NONE', ( #31683, #75315, #19849, #3050 ) ) ;
#85344=CARTESIAN_POINT ( 'NONE',  ( -86.52287095715006160, -24.66019654487199375, 8.947790411086119278 ) ) ;
#85345=CARTESIAN_POINT ( 'NONE',  ( -11.83016301840747175, -16.26703346747452983, -1.500000000000002220 ) ) ;
#85346=CARTESIAN_POINT ( 'NONE',  ( -16.48755246578841849, -13.11705038010048163, 11.49999999999999645 ) ) ;
#85347=CARTESIAN_POINT ( 'NONE',  ( -7.320055889550622474, -20.87099576385019972, 11.49999999999998934 ) ) ;
#85349=CARTESIAN_POINT ( 'NONE',  ( -20.41219973434085944, 2.133827299322149429, -1.500000000000002220 ) ) ;
#85351=CARTESIAN_POINT ( 'NONE',  ( -60.49713738156505372, -24.40034930558990922, 0.3402023900116026289 ) ) ;
#85352=ORIENTED_EDGE ( 'NONE', *, *, #70852, .F. ) ;
#85354=VERTEX_POINT ( 'NONE', #96186 ) ;
#85356=CARTESIAN_POINT ( 'NONE',  ( -102.5228709571500758, -23.47596703998600631, 11.44779298504228215 ) ) ;
#85357=ORIENTED_EDGE ( 'NONE', *, *, #32238, .T. ) ;
#85358=ORIENTED_EDGE ( 'NONE', *, *, #5388, .F. ) ;
#85359=ORIENTED_EDGE ( 'NONE', *, *, #65447, .F. ) ;
#85360=CARTESIAN_POINT ( 'NONE',  ( -117.2228709571500644, -23.47593901973090524, -1.443836447538996426 ) ) ;
#85361=CARTESIAN_POINT ( 'NONE',  ( -71.62287095715011276, -23.95044443724992789, 10.65354141964649415 ) ) ;
#85362=CARTESIAN_POINT ( 'NONE',  ( -68.50125515983249613, -24.35071581493542681, 9.817618358456032368 ) ) ;
#85363=B_SPLINE_CURVE_WITH_KNOTS ( 'NONE', 3,
 ( #82525, #83518, #50588, #67823, #35371, #36859 ),
 .UNSPECIFIED., .F., .F.,
 ( 4, 2, 4 ),
 ( 0.000000000000000000, 0.001380764517854764966, 0.002761529035709529931 ),
 .UNSPECIFIED. ) ;
#85364=CARTESIAN_POINT ( 'NONE',  ( -20.24099117049231467, 3.958469829285517161, -1.500000000000002220 ) ) ;
#85365=CARTESIAN_POINT ( 'NONE',  ( 19.98343133220876666, -8.209121646405339590, 11.49999999999999645 ) ) ;
#85367=CARTESIAN_POINT ( 'NONE',  ( -81.58953762381672448, -24.66019654487199020, 8.947790411086137041 ) ) ;
#85370=CARTESIAN_POINT ( 'NONE',  ( 1.438201247614206757, 22.34484416265529916, -1.500000000000002220 ) ) ;
#85371=LINE ( 'NONE', #15858, #14025 ) ;
#85372=DIRECTION ( 'NONE',  ( -3.773278334453079030E-23, 0.9999999999976377785, 2.173523156925979128E-06 ) ) ;
#85375=LINE ( 'NONE', #61565, #57229 ) ;
#85377=CARTESIAN_POINT ( 'NONE',  ( -12.66259425867894350, -16.64798919286708667, 11.49999999999998934 ) ) ;
#85379=PLANE ( 'NONE',  #32835 ) ;
#85380=B_SPLINE_CURVE_WITH_KNOTS ( 'NONE', 3,
 ( #12738, #13239, #16251, #45210, #8644, #39589, #77133, #99964, #45705, #78129, #69547, #47210, #525, #30474, #8146, #61440 ),
 .UNSPECIFIED., .F., .F.,
 ( 4, 2, 2, 2, 2, 2, 2, 4 ),
 ( 8.673617379884035472E-19, 0.0002961782169017380213, 0.0005923564338034751752, 0.0008885346507052124376, 0.001184712867606949483, 0.001777069301410424008, 0.002073247518312160836, 0.002369425735213897665 ),
 .UNSPECIFIED. ) ;
#85381=VERTEX_POINT ( 'NONE', #79447 ) ;
#85382=PLANE ( 'NONE',  #43889 ) ;
#85383=CARTESIAN_POINT ( 'NONE',  ( -19.98373207111551508, 7.008865001458166155, -1.500000000000002220 ) ) ;
#85385=CARTESIAN_POINT ( 'NONE',  ( -50.57926364954687415, -24.83618233451450408, 1.606449574219538601 ) ) ;
#85386=CARTESIAN_POINT ( 'NONE',  ( 9.495391690522565042, 19.61495305411445500, -1.500000000000002220 ) ) ;
#85387=CARTESIAN_POINT ( 'NONE',  ( -60.62287095715004881, -23.47596703998600631, 11.44779298504227505 ) ) ;
#85388=CARTESIAN_POINT ( 'NONE',  ( -76.56415518045969293, -23.48786465467240703, 11.44779295918254647 ) ) ;
#85389=CARTESIAN_POINT ( 'NONE',  ( -90.62287095715004170, -29.50249982740957577, 7.747779886224967605 ) ) ;
#85390=CARTESIAN_POINT ( 'NONE',  ( -1.743439162979827595, 21.76861016152796324, -1.500000000000002220 ) ) ;
#85393=EDGE_LOOP ( 'NONE', ( #34595, #1401, #43300, #97075 ) ) ;
#85396=ORIENTED_EDGE ( 'NONE', *, *, #20181, .F. ) ;
#85398=B_SPLINE_CURVE_WITH_KNOTS ( 'NONE', 3,
 ( #71466, #41011, #79563, #38998, #1954, #942 ),
 .UNSPECIFIED., .F., .F.,
 ( 4, 2, 4 ),
 ( 0.000000000000000000, 0.001380901958385379220, 0.002761803916770758441 ),
 .UNSPECIFIED. ) ;
#85399=ORIENTED_EDGE ( 'NONE', *, *, #3878, .T. ) ;
#85400=VERTEX_POINT ( 'NONE', #42419 ) ;
#85401=EDGE_CURVE ( 'NONE', #13466, #61820, #77859, .T. ) ;
#85402=CARTESIAN_POINT ( 'NONE',  ( -96.52287095715006160, -24.64965694238575011, 8.947790433994194714 ) ) ;
#85404=CARTESIAN_POINT ( 'NONE',  ( -19.96038302963917488, -7.207760892512529161, -1.500000000000002220 ) ) ;
#85405=CARTESIAN_POINT ( 'NONE',  ( -94.58862134658387788, -24.34968618360933945, 0.1864209137778861103 ) ) ;
#85407=CARTESIAN_POINT ( 'NONE',  ( -79.61785653407703478, -25.27791918801320037, 7.314036244604475989 ) ) ;
#85409=VECTOR ( 'NONE', #94834, 1000.000000000000114 ) ;
#85410=CARTESIAN_POINT ( 'NONE',  ( -39.04303308397305727, -25.29008967749855685, 4.215216926603018166 ) ) ;
#85411=CARTESIAN_POINT ( 'NONE',  ( 12.26431755764203047, -15.03328313062362298, 11.49999999999998934 ) ) ;
#85412=CARTESIAN_POINT ( 'NONE',  ( -51.90526032677228585, -25.28214432996132999, 5.906427834405539201 ) ) ;
#85414=CARTESIAN_POINT ( 'NONE',  ( 13.61561175257155298, 13.87280521877887018, 11.49999999999999645 ) ) ;
#85415=CARTESIAN_POINT ( 'NONE',  ( -26.33488822642538452, -24.89212854592702584, 6.524121854850513991 ) ) ;
#85417=CARTESIAN_POINT ( 'NONE',  ( -68.52287095715011844, -24.33832256527049154, 0.1851278514138628983 ) ) ;
#85422=CARTESIAN_POINT ( 'NONE',  ( -40.45829750704997707, -25.19502912051678223, 3.293943094755625633 ) ) ;
#85423=CARTESIAN_POINT ( 'NONE',  ( -93.62357236836618313, -24.66019654487200441, 8.947790411086105067 ) ) ;
#85424=CARTESIAN_POINT ( 'NONE',  ( -3.719764837209879271, -19.30396570740023421, 11.49999999999998934 ) ) ;
#85427=CARTESIAN_POINT ( 'NONE',  ( -21.50746323947805649, 1.722430922125298247, -1.500000000000002220 ) ) ;
#85428=CARTESIAN_POINT ( 'NONE',  ( -40.59317738058160074, -24.40034930558990922, 0.3402023900116037392 ) ) ;
#85430=CARTESIAN_POINT ( 'NONE',  ( -21.58539018223340022, -8.019882488244659768, -1.500000000000002220 ) ) ;
#85432=CARTESIAN_POINT ( 'NONE',  ( -93.58624035233277993, -24.51314013834316086, 0.6176544820404149538 ) ) ;
#85433=CARTESIAN_POINT ( 'NONE',  ( -90.52287095715009002, -24.14406661686762234, 10.28769366194075019 ) ) ;
#85434=CARTESIAN_POINT ( 'NONE',  ( -40.01839366089613748, -25.30501058306510487, 5.509688048021296858 ) ) ;
#85437=CARTESIAN_POINT ( 'NONE',  ( -111.3477393431454487, -25.10921465371560402, 3.253010550120815303 ) ) ;
#85438=CARTESIAN_POINT ( 'NONE',  ( -98.52287095715004739, -24.50216790748203977, 0.6166512839542589441 ) ) ;
#85439=CARTESIAN_POINT ( 'NONE',  ( -49.62287095715005592, -23.47593901973091235, -1.443836447539009749 ) ) ;
#85440=CARTESIAN_POINT ( 'NONE',  ( 19.87125486832220744, 0.9792442318621276121, 11.49999999999998934 ) ) ;
#85442=CARTESIAN_POINT ( 'NONE',  ( 6.388261542594571019, -18.74682169789839392, -1.500000000000002220 ) ) ;
#85446=CARTESIAN_POINT ( 'NONE',  ( -40.43756433397305727, -25.10925592397025241, 2.832404819646103800 ) ) ;
#85448=CARTESIAN_POINT ( 'NONE',  ( 1.212613378922696050, -20.72488358683818888, 11.49999999999999645 ) ) ;
#85449=AXIS2_PLACEMENT_3D ( 'NONE', #6798, #53993, #1203 ) ;
#85450=CARTESIAN_POINT ( 'NONE',  ( -106.6248962070219335, -24.51314013834316796, 0.6176544820404221703 ) ) ;
#85451=CARTESIAN_POINT ( 'NONE',  ( 6.015242202445381992, 21.98585358372262633, 11.49999999999999645 ) ) ;
#85452=EDGE_CURVE ( 'NONE', #5224, #94221, #61000, .T. ) ;
#85454=B_SPLINE_SURFACE_WITH_KNOTS ( 'NONE', 3, 3, ( 
 ( #69194, #83920, #14398, #30126 ),
 ( #76294, #61100, #22500, #100112 ),
 ( #1697, #10801, #40748, #86419 ),
 ( #87927, #2204, #18411, #86917 ),
 ( #25524, #78789, #48371, #33133 ),
 ( #64621, #41766, #80814, #17410 ),
 ( #9287, #79300, #64112, #49379 ),
 ( #41256, #9796, #72710, #63608 ),
 ( #95033, #2698, #80311, #56496 ),
 ( #3207, #32630, #34149, #65116 ) ),
 .UNSPECIFIED., .F., .F., .F.,
 ( 4, 3, 3, 4 ),
 ( 4, 4 ),
 ( 0.0004766839783810062465, 0.1491231665100168913, 0.2234464077758348266, 0.2977696490416527619 ),
 ( 0.8495966106698408238, 0.8511156054176940433 ),
 .UNSPECIFIED. ) ;
#85455=CARTESIAN_POINT ( 'NONE',  ( -69.50161766294181120, -24.34968618360934300, 0.1864209137778826408 ) ) ;
#85456=CARTESIAN_POINT ( 'NONE',  ( -74.62287095715005592, -24.51387760970724372, 9.387446482453425389 ) ) ;
#85457=ORIENTED_EDGE ( 'NONE', *, *, #93050, .T. ) ;
#85458=CARTESIAN_POINT ( 'NONE',  ( -18.82377384687745447, 7.257840063761761051, -1.500000000000002220 ) ) ;
#85459=CARTESIAN_POINT ( 'NONE',  ( -118.5228709571500758, -29.50250243563736774, 8.947779886222134493 ) ) ;
#85462=AXIS2_PLACEMENT_3D ( 'NONE', #47137, #16668, #85182 ) ;
#85465=CARTESIAN_POINT ( 'NONE',  ( -9.150087108448493822, 20.98025145036519845, -1.500000000000002220 ) ) ;
#85467=CARTESIAN_POINT ( 'NONE',  ( 21.64940796807912449, -0.2623997510114038922, -1.500000000000002220 ) ) ;
#85468=CARTESIAN_POINT ( 'NONE',  ( -36.62287095715004170, -23.47596703998600276, 11.44779298504227505 ) ) ;
#85469=CARTESIAN_POINT ( 'NONE',  ( -11.44352472427880052, 17.46665840655709090, 11.49999999999999645 ) ) ;
#85470=EDGE_LOOP ( 'NONE', ( #67914, #45809, #94430, #55731 ) ) ;
#85471=B_SPLINE_CURVE_WITH_KNOTS ( 'NONE', 3,
 ( #50933, #52425, #73757, #59542 ),
 .UNSPECIFIED., .F., .F.,
 ( 4, 4 ),
 ( 0.000000000000000000, 9.999999999998897304E-05 ),
 .UNSPECIFIED. ) ;
#85472=CARTESIAN_POINT ( 'NONE',  ( -124.5569027081732827, -23.48783264082477373, -1.443836473390086139 ) ) ;
#85473=CARTESIAN_POINT ( 'NONE',  ( -12.30081598482267680, 18.28176383447183895, 11.49999999999998934 ) ) ;
#85477=CARTESIAN_POINT ( 'NONE',  ( -65.62287095715005592, -24.51254535404254042, 9.355368623467647637 ) ) ;
#85479=CARTESIAN_POINT ( 'NONE',  ( -49.56515190845122021, -25.27344855749837294, 3.736414773304981285 ) ) ;
#85481=ORIENTED_EDGE ( 'NONE', *, *, #33075, .T. ) ;
#85482=LINE ( 'NONE', #6868, #11235 ) ;
#85484=VECTOR ( 'NONE', #95529, 1000.000000000000114 ) ;
#85487=CARTESIAN_POINT ( 'NONE',  ( -101.7667076177128678, -25.27404871335912517, 3.940951707345587973 ) ) ;
#85489=CARTESIAN_POINT ( 'NONE',  ( -7.951223608505463503, 18.87544906973805325, -1.500000000000002220 ) ) ;
#85494=CARTESIAN_POINT ( 'NONE',  ( -45.52287095715006160, -24.99156044556202616, 7.747789690856173195 ) ) ;
#85495=CARTESIAN_POINT ( 'NONE',  ( -13.27262489239681997, 17.90159134968837051, -1.500000000000002220 ) ) ;
#85497=CARTESIAN_POINT ( 'NONE',  ( -81.62287095715002749, -23.94994826722515668, -0.6494450866351701990 ) ) ;
#85499=ORIENTED_EDGE ( 'NONE', *, *, #77646, .F. ) ;
#85502=EDGE_CURVE ( 'NONE', #81363, #18101, #18573, .T. ) ;
#85503=CARTESIAN_POINT ( 'NONE',  ( -20.82185584224439978, -0.2524610531272265534, 11.49999999999998934 ) ) ;
#85506=ORIENTED_EDGE ( 'NONE', *, *, #7163, .F. ) ;
#85507=VERTEX_POINT ( 'NONE', #87567 ) ;
#85508=CARTESIAN_POINT ( 'NONE',  ( -50.85935151307011637, -25.25854555849183924, 7.039179658095172876 ) ) ;
#85509=CARTESIAN_POINT ( 'NONE',  ( -9.893913718187896222, 18.50344063021147889, -1.500000000000002220 ) ) ;
#85510=ORIENTED_EDGE ( 'NONE', *, *, #25512, .F. ) ;
#85511=CARTESIAN_POINT ( 'NONE',  ( -118.5228709571500616, -24.50321055353805377, 9.387540953477511607 ) ) ;
#85512=DIRECTION ( 'NONE',  ( 0.000000000000000000, 0.9999999999976377785, 2.173523156925979128E-06 ) ) ;
#85514=LINE ( 'NONE', #92130, #17770 ) ;
#85515=CARTESIAN_POINT ( 'NONE',  ( -92.54655063383911795, -24.51419770103157347, 9.386484678747171628 ) ) ;
#85516=CARTESIAN_POINT ( 'NONE',  ( -63.52287095715006160, -24.64898659630367561, 1.056161002820822592 ) ) ;
#85517=EDGE_CURVE ( 'NONE', #93507, #40340, #65755, .T. ) ;
#85518=CARTESIAN_POINT ( 'NONE',  ( -17.21897301287555848, -14.04741862099043104, 11.49999999999999645 ) ) ;
#85521=CARTESIAN_POINT ( 'NONE',  ( -49.52287095715006160, -29.50250243563736774, 8.947779886222146928 ) ) ;
#85523=CARTESIAN_POINT ( 'NONE',  ( -14.80616194778269623, -17.16973004002414882, 11.49999999999998934 ) ) ;
#85525=CARTESIAN_POINT ( 'NONE',  ( -28.60150425279314490, -24.94570498609691001, 7.235193128133280638 ) ) ;
#85526=ORIENTED_EDGE ( 'NONE', *, *, #21846, .F. ) ;
#85527=VERTEX_POINT ( 'NONE', #10436 ) ;
#85528=DIRECTION ( 'NONE',  ( 0.000000000000000000, -2.173523156925980399E-06, 0.9999999999976378895 ) ) ;
#85530=CARTESIAN_POINT ( 'NONE',  ( 14.76687977769557847, -13.71354340032049457, 11.49999999999998934 ) ) ;
#85532=CARTESIAN_POINT ( 'NONE',  ( -66.62287095715005592, -24.66019654487199020, 8.947790411086131712 ) ) ;
#85535=CARTESIAN_POINT ( 'NONE',  ( -18.48265707593502327, -12.51853143457666562, -1.500000000000002220 ) ) ;
#85536=ADVANCED_FACE ( 'NONE', ( #81949 ), #4340, .T. ) ;
#85537=ORIENTED_EDGE ( 'NONE', *, *, #24691, .F. ) ;
#85538=VERTEX_POINT ( 'NONE', #51510 ) ;
#85539=CARTESIAN_POINT ( 'NONE',  ( -35.52287095715006870, -23.47593901973090169, -1.443836447538997092 ) ) ;
#85540=CARTESIAN_POINT ( 'NONE',  ( -94.51006116474896146, -24.35071581493543036, 9.817618358456030592 ) ) ;
#85541=CARTESIAN_POINT ( 'NONE',  ( -54.62287095715004170, -23.47596703998600631, 11.44779298504227505 ) ) ;
#85542=PLANE ( 'NONE',  #4435 ) ;
#85543=VECTOR ( 'NONE', #96673, 1000.000000000000114 ) ;
#85544=EDGE_CURVE ( 'NONE', #25617, #91623, #6321, .T. ) ;
#85545=CARTESIAN_POINT ( 'NONE',  ( -63.95380932530888884, -23.47593901973090169, -1.443836447538997758 ) ) ;
#85546=CARTESIAN_POINT ( 'NONE',  ( 17.64699390344983598, -8.409456921668478913, 11.49999999999998934 ) ) ;
#85548=CARTESIAN_POINT ( 'NONE',  ( -0.7226137440361984909, -21.50112622129444162, -1.500000000000002220 ) ) ;
#85549=CARTESIAN_POINT ( 'NONE',  ( -128.6240058187065927, -23.96119346886882084, -0.6495511937831803806 ) ) ;
#85551=DIRECTION ( 'NONE',  ( -3.773278334453079030E-23, 0.9999999999976377785, 2.173523156925979128E-06 ) ) ;
#85552=CARTESIAN_POINT ( 'NONE',  ( -80.62287095715004170, -24.62285846362213348, 9.038163152653524435 ) ) ;
#85553=CARTESIAN_POINT ( 'NONE',  ( 9.452765381649220089, 20.79790602042944414, -1.500000000000002220 ) ) ;
#85554=VECTOR ( 'NONE', #53941, 1000.000000000000227 ) ;
#85555=B_SPLINE_CURVE_WITH_KNOTS ( 'NONE', 3,
 ( #94005, #8779, #39217, #23991, #64093, #40232 ),
 .UNSPECIFIED., .F., .F.,
 ( 4, 2, 4 ),
 ( 1.570755371633875854E-05, 0.001396183895866087753, 0.002776660238015836446 ),
 .UNSPECIFIED. ) ;
#85558=CARTESIAN_POINT ( 'NONE',  ( -53.55343082792221310, -23.96119346886879953, -0.6495511937832126881 ) ) ;
#85559=CARTESIAN_POINT ( 'NONE',  ( -16.84340083857899018, -10.81494551495373457, 11.49999999999999645 ) ) ;
#85560=CARTESIAN_POINT ( 'NONE',  ( -79.24831702480813078, -25.31594428705783528, 5.024332805295591342 ) ) ;
#85564=LINE ( 'NONE', #40898, #18096 ) ;
#85565=ORIENTED_EDGE ( 'NONE', *, *, #40780, .F. ) ;
#85566=CARTESIAN_POINT ( 'NONE',  ( -79.34687923781922336, -25.27781941911278807, 5.960409260969139922 ) ) ;
#85567=CARTESIAN_POINT ( 'NONE',  ( 19.96715809174937561, -8.635335823514383335, -1.500000000000002220 ) ) ;
#85568=PLANE ( 'NONE',  #78716 ) ;
#85569=CARTESIAN_POINT ( 'NONE',  ( -19.67010641940559168, 0.002901314006966619011, -1.500000000000002220 ) ) ;
#85570=DIRECTION ( 'NONE',  ( -3.773278334453079030E-23, 0.9999999999976377785, 2.173523156925978705E-06 ) ) ;
#85572=CARTESIAN_POINT ( 'NONE',  ( -41.41142090293942601, -25.25399135992076083, 3.882215004696675908 ) ) ;
#85574=CARTESIAN_POINT ( 'NONE',  ( -38.62287095715005592, -23.47596703998600276, 11.44779298504227505 ) ) ;
#85575=CARTESIAN_POINT ( 'NONE',  ( -92.52287095715006160, -29.50250786944525672, 11.44777988621623344 ) ) ;
#85576=CARTESIAN_POINT ( 'NONE',  ( 11.93631617611541351, -16.73449621718459923, 11.49999999999999645 ) ) ;
#85577=CARTESIAN_POINT ( 'NONE',  ( -94.52287095715000476, -23.94994826722564341, -0.6494450866342716955 ) ) ;
#85578=CARTESIAN_POINT ( 'NONE',  ( -120.5196240066739648, -24.15503026093913874, -0.2815557561904507011 ) ) ;
#85579=CARTESIAN_POINT ( 'NONE',  ( -22.55165446212525993, 1.111233042438415808, 11.49999999999999645 ) ) ;
#85582=CARTESIAN_POINT ( 'NONE',  ( -100.2051565992114632, -25.31296438552667993, 4.680112719389787124 ) ) ;
#85583=LINE ( 'NONE', #33296, #745 ) ;
#85584=CARTESIAN_POINT ( 'NONE',  ( -125.5202163252652525, -24.52399227489127043, 9.353111116836528183 ) ) ;
#85586=CARTESIAN_POINT ( 'NONE',  ( -25.63919700385670453, -24.61459675201335173, 6.233790649395326788 ) ) ;
#85588=VERTEX_POINT ( 'NONE', #36778 ) ;
#85589=CARTESIAN_POINT ( 'NONE',  ( -3.381418692465893105, -22.81955385325859709, 11.49999999999999645 ) ) ;
#85590=CARTESIAN_POINT ( 'NONE',  ( 20.42703387425654427, 10.12935691860780985, 11.49999999999998934 ) ) ;
#85591=CARTESIAN_POINT ( 'NONE',  ( -74.54989380979742464, -24.15543982623906771, -0.2315651400026650653 ) ) ;
#85592=B_SPLINE_SURFACE_WITH_KNOTS ( 'NONE', 3, 3, ( 
 ( #44656, #7583, #82707, #29416 ),
 ( #69490, #92811, #98925, #29918 ),
 ( #53774, #60885, #13184, #100407 ),
 ( #91319, #21791, #22289, #53270 ),
 ( #67998, #28922, #84200, #36531 ),
 ( #52767, #6584, #99424, #46155 ),
 ( #13686, #98420, #59893, #91814 ) ),
 .UNSPECIFIED., .F., .F., .F.,
 ( 4, 3, 4 ),
 ( 4, 4 ),
 ( 0.7945040050992243641, 0.8970133687736501216, 0.9995227324480757680 ),
 ( 0.2795650385958281525, 0.2807068289243159764 ),
 .UNSPECIFIED. ) ;
#85594=CARTESIAN_POINT ( 'NONE',  ( -89.52287095715006160, -23.47596703998600631, 11.44779298504228393 ) ) ;
#85595=CARTESIAN_POINT ( 'NONE',  ( -16.84940295534276800, 14.81145437567392698, 11.49999999999999645 ) ) ;
#85597=CARTESIAN_POINT ( 'NONE',  ( -40.01839366089613748, -29.50249496284529727, 5.509678924691796098 ) ) ;
#85599=CARTESIAN_POINT ( 'NONE',  ( -21.49438740719132923, 4.340694165963498996, 11.49999999999998934 ) ) ;
#85600=CARTESIAN_POINT ( 'NONE',  ( -54.62287095715004881, -23.48783264082478084, -1.443836473390070596 ) ) ;
#85602=CARTESIAN_POINT ( 'NONE',  ( -34.53824809528569517, -24.35071581493542681, 9.817618358456032368 ) ) ;
#85604=EDGE_LOOP ( 'NONE', ( #66992, #46452, #41066, #70547 ) ) ;
#85605=CARTESIAN_POINT ( 'NONE',  ( -48.93000761175007796, -25.20616604562876617, 6.556111049017001591 ) ) ;
#85606=DIRECTION ( 'NONE',  ( -3.773278334453079030E-23, 0.9999999999976377785, 2.173523156925979128E-06 ) ) ;
#85607=VERTEX_POINT ( 'NONE', #59625 ) ;
#85608=CARTESIAN_POINT ( 'NONE',  ( 12.80116962295325322, 15.99954467330607244, 11.49999999999998934 ) ) ;
#85609=EDGE_LOOP ( 'NONE', ( #33962, #95659, #82245, #54814 ) ) ;
#85611=VERTEX_POINT ( 'NONE', #27673 ) ;
#85613=CARTESIAN_POINT ( 'NONE',  ( -20.32320236877023589, 10.94715076914730290, -1.500000000000002220 ) ) ;
#85614=CARTESIAN_POINT ( 'NONE',  ( -49.37922875195936001, -25.19117186706260014, 3.263664075997171121 ) ) ;
#85615=CARTESIAN_POINT ( 'NONE',  ( -15.70679263237263434, -12.88635299011707502, -1.500000000000002220 ) ) ;
#85620=AXIS2_PLACEMENT_3D ( 'NONE', #5459, #22164, #83573 ) ;
#85621=CARTESIAN_POINT ( 'NONE',  ( -92.63387814436620715, -23.96119346886881374, -0.6495511937831873750 ) ) ;
#85623=B_SPLINE_CURVE_WITH_KNOTS ( 'NONE', 3,
 ( #28176, #83443, #14430, #21044, #38268, #67749 ),
 .UNSPECIFIED., .F., .F.,
 ( 4, 2, 4 ),
 ( 6.391158118972359742E-06, 0.001387004593080793302, 0.002767618028042614139 ),
 .UNSPECIFIED. ) ;
#85625=CARTESIAN_POINT ( 'NONE',  ( -70.62368311109368335, -25.00158670708910691, 2.256160236439221034 ) ) ;
#85626=CARTESIAN_POINT ( 'NONE',  ( -19.93307770644097232, -8.117153041090405807, 11.49999999999999645 ) ) ;
#85627=ORIENTED_EDGE ( 'NONE', *, *, #70392, .F. ) ;
#85628=CARTESIAN_POINT ( 'NONE',  ( -125.5895376238167245, -24.99132157543083821, 2.256160258750496528 ) ) ;
#85631=ORIENTED_EDGE ( 'NONE', *, *, #63941, .T. ) ;
#85632=CARTESIAN_POINT ( 'NONE',  ( -2.856624844580134770, 20.53689577262001364, 11.49999999999998934 ) ) ;
#85633=ORIENTED_EDGE ( 'NONE', *, *, #91231, .T. ) ;
#85635=VERTEX_POINT ( 'NONE', #20051 ) ;
#85636=CARTESIAN_POINT ( 'NONE',  ( -111.6321636762771448, -23.48786465467241769, 11.44779295918254114 ) ) ;
#85637=CARTESIAN_POINT ( 'NONE',  ( -43.62287095715004881, -29.50250243563736774, 8.947779886222148704 ) ) ;
#85638=ORIENTED_EDGE ( 'NONE', *, *, #76585, .F. ) ;
#85640=LINE ( 'NONE', #31864, #46179 ) ;
#85642=AXIS2_PLACEMENT_3D ( 'NONE', #35922, #60772, #14069 ) ;
#85643=B_SPLINE_CURVE_WITH_KNOTS ( 'NONE', 3,
 ( #63822, #94233, #88139, #55197 ),
 .UNSPECIFIED., .F., .F.,
 ( 4, 4 ),
 ( 0.000000000000000000, 9.999999999998897304E-05 ),
 .UNSPECIFIED. ) ;
#85644=CARTESIAN_POINT ( 'NONE',  ( -117.5228709571500758, -23.47596703998600631, 11.44779298504227860 ) ) ;
#85645=B_SPLINE_CURVE_WITH_KNOTS ( 'NONE', 3,
 ( #89970, #20445, #37180, #45301, #68136, #15827 ),
 .UNSPECIFIED., .F., .F.,
 ( 4, 2, 4 ),
 ( 1.570755371633836552E-05, 0.001396183895866087753, 0.002776660238015836880 ),
 .UNSPECIFIED. ) ;
#85646=CARTESIAN_POINT ( 'NONE',  ( -76.52287095715007581, -24.66019654487199730, 8.947790411086124607 ) ) ;
#85648=EDGE_CURVE ( 'NONE', #71695, #47216, #13924, .T. ) ;
#85649=CARTESIAN_POINT ( 'NONE',  ( 13.08019894233326319, 17.74467248152726384, 11.49999999999999645 ) ) ;
#85651=CARTESIAN_POINT ( 'NONE',  ( 21.27769986149581172, 7.469961712261545372, 11.49999999999998934 ) ) ;
#85652=CARTESIAN_POINT ( 'NONE',  ( 20.99820426035194032, -0.1900765340283884497, 11.49999999999998934 ) ) ;
#85655=EDGE_CURVE ( 'NONE', #51201, #10079, #19641, .T. ) ;
#85657=ORIENTED_EDGE ( 'NONE', *, *, #93238, .F. ) ;
#85658=CARTESIAN_POINT ( 'NONE',  ( -80.62287095715004170, -24.91544648472620338, 1.928969306349224810 ) ) ;
#85662=CARTESIAN_POINT ( 'NONE',  ( 19.19679251752027227, 8.867671107084703408, 11.49999999999998934 ) ) ;
#85664=CARTESIAN_POINT ( 'NONE',  ( -51.83680534327738343, -25.26040924062689896, 6.675008265709720057 ) ) ;
#85665=CARTESIAN_POINT ( 'NONE',  ( -88.62287095715004170, -23.47596703998600631, 11.44779298504227860 ) ) ;
#85666=DIRECTION ( 'NONE',  ( -3.773278334453079030E-23, 0.9999999999976377785, 2.173523156925979128E-06 ) ) ;
#85668=CARTESIAN_POINT ( 'NONE',  ( -10.56713949322891999, -19.48831581008217384, -1.500000000000002220 ) ) ;
#85669=CARTESIAN_POINT ( 'NONE',  ( -71.54135322174539624, -24.51314013834315730, 0.6176544820404130665 ) ) ;
#85672=CARTESIAN_POINT ( 'NONE',  ( -51.77186309286971522, -25.24860127752034700, 5.562993739656123537 ) ) ;
#85673=CARTESIAN_POINT ( 'NONE',  ( -37.52201680321181243, -23.48783264082477729, -1.443836473390075703 ) ) ;
#85674=CARTESIAN_POINT ( 'NONE',  ( -126.5547695978490310, -24.65952944569306027, 1.056160979905708786 ) ) ;
#85675=EDGE_CURVE ( 'NONE', #80353, #8894, #66255, .T. ) ;
#85678=B_SPLINE_CURVE_WITH_KNOTS ( 'NONE', 3,
 ( #97447, #59900, #82713, #45169 ),
 .UNSPECIFIED., .F., .F.,
 ( 4, 4 ),
 ( 0.000000000000000000, 1.000000000000000000 ),
 .UNSPECIFIED. ) ;
#85680=CARTESIAN_POINT ( 'NONE',  ( 15.33136405852079243, -11.96835230219363311, -1.500000000000002220 ) ) ;
#85681=CARTESIAN_POINT ( 'NONE',  ( -17.32345979880200204, -12.59856583755568415, 11.49999999999998934 ) ) ;
#85682=CARTESIAN_POINT ( 'NONE',  ( -62.62751418018152094, -24.51314013834316441, 0.6176544820404141767 ) ) ;
#85685=CARTESIAN_POINT ( 'NONE',  ( -101.3603016561062589, -25.27360118438346248, 3.955748476195026342 ) ) ;
#85686=CARTESIAN_POINT ( 'NONE',  ( -17.38503614929206265, -14.63273120789127013, -1.500000000000002220 ) ) ;
#85687=B_SPLINE_SURFACE_WITH_KNOTS ( 'NONE', 3, 3, ( 
 ( #57914, #3622, #88858, #49806 ),
 ( #26946, #34066, #56418, #87337 ),
 ( #50295, #73130, #80738, #19323 ),
 ( #87850, #34569, #81232, #11710 ),
 ( #73624, #48802, #4116, #35065 ),
 ( #80232, #96955, #56917, #64041 ),
 ( #94956, #79724, #72635, #41178 ) ),
 .UNSPECIFIED., .F., .F., .F.,
 ( 4, 3, 4 ),
 ( 4, 4 ),
 ( 0.0004766839783816872339, 0.1029713700210893590, 0.2054660560637970312 ),
 ( 0.5696389036532559791, 0.5709144585527624605 ),
 .UNSPECIFIED. ) ;
#85688=CARTESIAN_POINT ( 'NONE',  ( -98.51627647636760798, -23.96119346886880663, -0.6495511937832080251 ) ) ;
#85689=CARTESIAN_POINT ( 'NONE',  ( -58.52287095715006160, -29.50250243563736774, 8.947779886222145151 ) ) ;
#85690=CARTESIAN_POINT ( 'NONE',  ( 11.24879072547334324, 16.40116332625411033, 11.49999999999999645 ) ) ;
#85691=CARTESIAN_POINT ( 'NONE',  ( -123.5563712641698118, -23.73791477778912196, 11.05961554403169878 ) ) ;
#85692=VECTOR ( 'NONE', #85222, 1000.000000000000114 ) ;
#85693=AXIS2_PLACEMENT_3D ( 'NONE', #59220, #65860, #96778 ) ;
#85696=CARTESIAN_POINT ( 'NONE',  ( -49.53207283835729413, -25.17696084702891568, 6.767063398092357573 ) ) ;
#85698=B_SPLINE_CURVE_WITH_KNOTS ( 'NONE', 3,
 ( #70347, #25160, #55132, #830 ),
 .UNSPECIFIED., .F., .F.,
 ( 4, 4 ),
 ( 0.000000000000000000, 9.999999999998897304E-05 ),
 .UNSPECIFIED. ) ;
#85699=CARTESIAN_POINT ( 'NONE',  ( -51.66021737866784491, -25.10935945577014294, 3.699308914517982938 ) ) ;
#85700=CARTESIAN_POINT ( 'NONE',  ( -20.56447267657262401, 6.860157381912782348, 11.49999999999998934 ) ) ;
#85701=CARTESIAN_POINT ( 'NONE',  ( -66.55620429048339304, -24.65952944569304606, 1.056160979905697905 ) ) ;
#85703=CARTESIAN_POINT ( 'NONE',  ( 1.793504005174451077, 19.40006364325761012, -1.500000000000002220 ) ) ;
#85707=CARTESIAN_POINT ( 'NONE',  ( -19.47531982339030776, -5.969937916086089480, 11.49999999999999645 ) ) ;
#85709=DIRECTION ( 'NONE',  ( -3.773278334453079030E-23, 0.9999999999976377785, 2.173523156925979128E-06 ) ) ;
#85710=ORIENTED_EDGE ( 'NONE', *, *, #13678, .F. ) ;
#85711=CARTESIAN_POINT ( 'NONE',  ( -40.58336788261102157, -25.19566465339486783, 3.298403319262286360 ) ) ;
#85712=CARTESIAN_POINT ( 'NONE',  ( -92.52287095715006160, -23.47593901973090169, -1.443836447538996426 ) ) ;
#85713=CARTESIAN_POINT ( 'NONE',  ( -59.80072539166535250, -25.14083923594767001, 2.947789366383931853 ) ) ;
#85715=CARTESIAN_POINT ( 'NONE',  ( -128.6228709571500701, -24.51283580621365843, 0.6167428607019860287 ) ) ;
#85717=CARTESIAN_POINT ( 'NONE',  ( -0.3114230556345199963, -20.10660241673355486, -1.500000000000002220 ) ) ;
#85718=CARTESIAN_POINT ( 'NONE',  ( -57.55620429048340725, -23.47593901973091235, -1.443836447539007972 ) ) ;
#85720=CARTESIAN_POINT ( 'NONE',  ( -91.62287095715004170, -23.96177878511308634, 10.65340807706329507 ) ) ;
#85721=CARTESIAN_POINT ( 'NONE',  ( 22.59171682324826236, -3.780823453261925593, 11.49999999999999645 ) ) ;
#85722=CARTESIAN_POINT ( 'NONE',  ( -17.38503614929206265, -14.63273120789127013, 11.49999999999998934 ) ) ;
#85723=ORIENTED_EDGE ( 'NONE', *, *, #98689, .F. ) ;
#85724=CARTESIAN_POINT ( 'NONE',  ( -45.52287095715006870, -24.63287334234177450, 0.9662140553045317493 ) ) ;
#85727=CARTESIAN_POINT ( 'NONE',  ( -30.57287095715005520, -24.67790239037960021, 8.895694439986561619 ) ) ;
#85730=CARTESIAN_POINT ( 'NONE',  ( -98.89303308397303738, -25.31200744192977581, 6.110950052045652114 ) ) ;
#85732=ADVANCED_FACE ( 'NONE', ( #46887 ), #62617, .T. ) ;
#85733=CARTESIAN_POINT ( 'NONE',  ( 18.38310620586021571, 8.829655622120887060, 11.49999999999998934 ) ) ;
#85734=ORIENTED_EDGE ( 'NONE', *, *, #3762, .F. ) ;
#85735=EDGE_CURVE ( 'NONE', #7838, #44949, #66938, .T. ) ;
#85736=CARTESIAN_POINT ( 'NONE',  ( 4.903590608199674072, 22.46510890469962263, 11.49999999999998934 ) ) ;
#85737=CARTESIAN_POINT ( 'NONE',  ( -69.22287095715007865, -23.47596703998600276, 11.44779298504227860 ) ) ;
#85738=EDGE_CURVE ( 'NONE', #3935, #27247, #2771, .T. ) ;
#85740=CARTESIAN_POINT ( 'NONE',  ( -114.5228709571501184, -24.35013146730204525, 9.818937971375092388 ) ) ;
#85741=EDGE_CURVE ( 'NONE', #10167, #42367, #40321, .T. ) ;
#85742=CARTESIAN_POINT ( 'NONE',  ( -84.62287095715002749, -23.96127896941631619, -0.6493128931037801532 ) ) ;
#85744=CARTESIAN_POINT ( 'NONE',  ( -89.58953762381671027, -24.65952944569304961, 1.056160979905700126 ) ) ;
#85745=CARTESIAN_POINT ( 'NONE',  ( -16.05942832139214360, -14.02155611864158402, 11.49999999999999645 ) ) ;
#85746=VERTEX_POINT ( 'NONE', #61627 ) ;
#85748=CARTESIAN_POINT ( 'NONE',  ( -2.516727866726558460, 22.04588476715296963, 11.49999999999998934 ) ) ;
#85749=CARTESIAN_POINT ( 'NONE',  ( -3.285303218690974525, -20.39892020120133154, -1.500000000000002220 ) ) ;
#85750=ORIENTED_EDGE ( 'NONE', *, *, #89531, .T. ) ;
#85751=EDGE_LOOP ( 'NONE', ( #28149, #50000, #7648, #5493 ) ) ;
#85753=CARTESIAN_POINT ( 'NONE',  ( -95.64416487886954599, -23.48786465467241058, 11.44779295918254469 ) ) ;
#85754=VERTEX_POINT ( 'NONE', #84936 ) ;
#85755=CARTESIAN_POINT ( 'NONE',  ( -91.50436023160280286, -24.65952944569304606, 1.056160979905703234 ) ) ;
#85756=VECTOR ( 'NONE', #35321, 1000.000000000000114 ) ;
#85758=CARTESIAN_POINT ( 'NONE',  ( -58.54813711902425410, -24.15620529776628089, 10.23563542870660470 ) ) ;
#85759=DIRECTION ( 'NONE',  ( -3.773278334453079618E-23, 0.9999999999976377785, 2.173523156925978705E-06 ) ) ;
#85760=CARTESIAN_POINT ( 'NONE',  ( 5.579783289733251550, -20.15082174716252794, -1.500000000000002220 ) ) ;
#85761=EDGE_CURVE ( 'NONE', #54721, #97694, #76808, .T. ) ;
#85762=CARTESIAN_POINT ( 'NONE',  ( 21.83686239284238084, -0.8075297431944471471, 11.49999999999999645 ) ) ;
#85763=CARTESIAN_POINT ( 'NONE',  ( -27.61674701359889639, -24.77993797186285008, 7.602796574010316277 ) ) ;
#85764=CARTESIAN_POINT ( 'NONE',  ( -78.50858408022973833, -24.15620529776628445, 10.23563542870660292 ) ) ;
#85765=CARTESIAN_POINT ( 'NONE',  ( 11.54466316424315231, -19.26756404802103972, -1.500000000000002220 ) ) ;
#85767=CARTESIAN_POINT ( 'NONE',  ( -38.56988824117014758, -23.48783264082477729, -1.443836473390076591 ) ) ;
#85768=CARTESIAN_POINT ( 'NONE',  ( -87.55620429048337883, -23.48783264082478084, -1.443836473390063269 ) ) ;
#85770=ADVANCED_FACE ( 'NONE', ( #15421 ), #77314, .F. ) ;
#85771=AXIS2_PLACEMENT_3D ( 'NONE', #8366, #29213, #69775 ) ;
#85774=ORIENTED_EDGE ( 'NONE', *, *, #20550, .T. ) ;
#85775=B_SPLINE_CURVE_WITH_KNOTS ( 'NONE', 3,
 ( #53899, #15314, #85328, #24434 ),
 .UNSPECIFIED., .F., .F.,
 ( 4, 4 ),
 ( 0.000000000000000000, 0.0001000000000000028644 ),
 .UNSPECIFIED. ) ;
#85776=EDGE_LOOP ( 'NONE', ( #85565, #58181, #24784, #38063 ) ) ;
#85777=B_SPLINE_CURVE_WITH_KNOTS ( 'NONE', 3,
 ( #76494, #84621, #82621, #75999 ),
 .UNSPECIFIED., .F., .F.,
 ( 4, 4 ),
 ( 1.387778780781445676E-17, 0.0001000000000000028508 ),
 .UNSPECIFIED. ) ;
#85779=CARTESIAN_POINT ( 'NONE',  ( -20.51402961445061734, 6.013860829077147585, -1.500000000000002220 ) ) ;
#85780=CARTESIAN_POINT ( 'NONE',  ( 15.07672925556244969, 16.42598562245719407, 11.49999999999999645 ) ) ;
#85782=CARTESIAN_POINT ( 'NONE',  ( -21.07084664159375009, 0.3847054351051909515, -1.500000000000002220 ) ) ;
#85783=CARTESIAN_POINT ( 'NONE',  ( -30.42979910109433916, -24.56868136509832112, 0.8299800598022502029 ) ) ;
#85784=CARTESIAN_POINT ( 'NONE',  ( -12.66726347749767179, -15.43046242340049545, -1.500000000000002220 ) ) ;
#85785=CARTESIAN_POINT ( 'NONE',  ( -50.53276790146632891, -24.73531770709094602, 8.716586749053508498 ) ) ;
#85786=CARTESIAN_POINT ( 'NONE',  ( -49.36964668519517829, -25.11052413561256813, 7.227227948084789411 ) ) ;
#85787=CARTESIAN_POINT ( 'NONE',  ( 1.410849576418898632, -21.91845101833037290, -1.500000000000002220 ) ) ;
#85788=CARTESIAN_POINT ( 'NONE',  ( -76.58953762381673869, -24.65952944569304606, 1.056160979905704123 ) ) ;
#85792=CARTESIAN_POINT ( 'NONE',  ( 16.20321855003292555, -13.12800272717607619, 11.49999999999999645 ) ) ;
#85793=ADVANCED_FACE ( 'NONE', ( #78315 ), #37198, .T. ) ;
#85795=B_SPLINE_CURVE_WITH_KNOTS ( 'NONE', 3,
 ( #94043, #24528, #20287, #81209 ),
 .UNSPECIFIED., .F., .F.,
 ( 4, 4 ),
 ( 0.000000000000000000, 9.999999999997510880E-05 ),
 .UNSPECIFIED. ) ;
#85796=CARTESIAN_POINT ( 'NONE',  ( -125.5228709571501184, -24.51254535375844057, 9.355368624242190734 ) ) ;
#85798=CARTESIAN_POINT ( 'NONE',  ( -21.20786952941880443, -2.223526401999901925, -1.500000000000002220 ) ) ;
#85799=CARTESIAN_POINT ( 'NONE',  ( -98.55771473076809741, -23.73791477778912196, 11.05961554403170588 ) ) ;
#85800=DIRECTION ( 'NONE',  ( -3.773278334453080206E-23, 0.9999999999976377785, 2.173523156925979975E-06 ) ) ;
#85801=ADVANCED_FACE ( 'NONE', ( #65135 ), #48387, .T. ) ;
#85802=CARTESIAN_POINT ( 'NONE',  ( -110.9353407762807251, -25.06732983082694943, 7.447789526168955732 ) ) ;
#85804=CARTESIAN_POINT ( 'NONE',  ( 5.133194422563156500, 21.89913303424002677, -1.500000000000002220 ) ) ;
#85805=DIRECTION ( 'NONE',  ( 0.000000000000000000, 0.9999999999976377785, 2.173523156925979975E-06 ) ) ;
#85806=ORIENTED_EDGE ( 'NONE', *, *, #34831, .T. ) ;
#85807=CARTESIAN_POINT ( 'NONE',  ( -79.88859889895181254, -25.29802671295835026, 4.572338242537191455 ) ) ;
#85808=CARTESIAN_POINT ( 'NONE',  ( -31.48872353745126773, -24.35071581493542325, 9.817618358456039473 ) ) ;
#85809=CARTESIAN_POINT ( 'NONE',  ( -16.89733858281218204, -10.06102416988892934, 11.49999999999999645 ) ) ;
#85812=ORIENTED_EDGE ( 'NONE', *, *, #69351, .F. ) ;
#85813=CARTESIAN_POINT ( 'NONE',  ( -99.56067757241656579, -23.48783264082478439, -1.443836473390063047 ) ) ;
#85815=CARTESIAN_POINT ( 'NONE',  ( -124.5888231589337209, -24.66019654487200441, 8.947790411086108620 ) ) ;
#85817=CARTESIAN_POINT ( 'NONE',  ( -0.6023826358649750912, 19.72334862104828090, 11.49999999999998934 ) ) ;
#85822=ORIENTED_EDGE ( 'NONE', *, *, #17875, .F. ) ;
#85823=DIRECTION ( 'NONE',  ( 0.000000000000000000, 0.9999999999976377785, 2.173523156925979128E-06 ) ) ;
#85824=DIRECTION ( 'NONE',  ( 3.773278334444167608E-23, -1.000000000000000000, 0.000000000000000000 ) ) ;
#85829=CARTESIAN_POINT ( 'NONE',  ( -41.55620429048340014, -24.66019654487199020, 8.947790411086135265 ) ) ;
#85830=CARTESIAN_POINT ( 'NONE',  ( -40.49165087243459737, -25.30353303947430987, 5.543942858925161588 ) ) ;
#85831=CARTESIAN_POINT ( 'NONE',  ( -7.547287378330592489, -18.53391252851691462, -1.500000000000002220 ) ) ;
#85832=PLANE ( 'NONE',  #15943 ) ;
#85834=ORIENTED_EDGE ( 'NONE', *, *, #18627, .F. ) ;
#85836=VECTOR ( 'NONE', #31861, 1000.000000000000114 ) ;
#85837=CARTESIAN_POINT ( 'NONE',  ( -79.52213156321093379, -23.48786465467241058, 11.44779295918254824 ) ) ;
#85838=CARTESIAN_POINT ( 'NONE',  ( -109.3584176993576591, -25.18430352096120473, 4.206202733454734499 ) ) ;
#85839=CARTESIAN_POINT ( 'NONE',  ( -35.65502281178025612, -24.15503026093914940, -0.2815557561904327155 ) ) ;
#85840=CARTESIAN_POINT ( 'NONE',  ( -100.5228709571500332, -24.15516710230296482, 10.28746687063728160 ) ) ;
#85843=PLANE ( 'NONE',  #79363 ) ;
#85844=AXIS2_PLACEMENT_3D ( 'NONE', #71183, #64092, #25501 ) ;
#85845=CARTESIAN_POINT ( 'NONE',  ( -63.62287095715004881, -23.96177878511307568, 10.65340807706329862 ) ) ;
#85846=CARTESIAN_POINT ( 'NONE',  ( -44.62287095715004881, -29.50250786944525672, 11.44777988621624232 ) ) ;
#85847=EDGE_LOOP ( 'NONE', ( #67192, #85734, #53459, #44582 ) ) ;
#85848=CARTESIAN_POINT ( 'NONE',  ( -18.37190169643047355, -11.86832528159398237, -1.500000000000002220 ) ) ;
#85849=EDGE_CURVE ( 'NONE', #94640, #42958, #78944, .T. ) ;
#85850=CARTESIAN_POINT ( 'NONE',  ( 18.82434097252966154, -7.598309640217090433, -1.500000000000002220 ) ) ;
#85853=CARTESIAN_POINT ( 'NONE',  ( -52.62287095715005592, -29.50247984919015209, -1.443849546365058689 ) ) ;
#85854=EDGE_CURVE ( 'NONE', #45470, #100015, #48894, .T. ) ;
#85855=ORIENTED_EDGE ( 'NONE', *, *, #84368, .F. ) ;
#85857=CARTESIAN_POINT ( 'NONE',  ( 9.931738293602487389, -17.53800358597336384, -1.500000000000002220 ) ) ;
#85858=B_SPLINE_CURVE_WITH_KNOTS ( 'NONE', 3,
 ( #842, #39901, #7949, #24172 ),
 .UNSPECIFIED., .F., .F.,
 ( 4, 4 ),
 ( 0.000000000000000000, 9.999999999998897304E-05 ),
 .UNSPECIFIED. ) ;
#85859=ADVANCED_FACE ( 'NONE', ( #80835 ), #88450, .F. ) ;
#85860=CARTESIAN_POINT ( 'NONE',  ( -21.09505027744838657, -1.104435277493458045, 11.49999999999999645 ) ) ;
#85861=CARTESIAN_POINT ( 'NONE',  ( 16.06085343747454175, -15.19291221174989204, -1.500000000000002220 ) ) ;
#85862=EDGE_CURVE ( 'NONE', #55233, #81363, #83796, .T. ) ;
#85863=CARTESIAN_POINT ( 'NONE',  ( -6.092534927433182368, -19.63929903328317295, -1.500000000000002220 ) ) ;
#85864=CARTESIAN_POINT ( 'NONE',  ( -60.63671166649558586, -24.52300882791528380, 0.6510814631126233820 ) ) ;
#85865=ORIENTED_EDGE ( 'NONE', *, *, #45430, .T. ) ;
#85868=DIRECTION ( 'NONE',  ( 1.000000000000000000, 3.773278334444166432E-23, 8.201307841325785021E-29 ) ) ;
#85869=CARTESIAN_POINT ( 'NONE',  ( -109.5228709571500332, -24.50321055353806088, 9.387540953477524042 ) ) ;
#85870=EDGE_LOOP ( 'NONE', ( #3553, #66726, #92349, #68166 ) ) ;
#85872=EDGE_LOOP ( 'NONE', ( #74794, #22939, #69560, #29093 ) ) ;
#85873=CARTESIAN_POINT ( 'NONE',  ( -100.5228709571500474, -24.91544648472620693, 1.928969306349232582 ) ) ;
#85874=DIRECTION ( 'NONE',  ( 0.000000000000000000, 2.173523156925980399E-06, -0.9999999999976378895 ) ) ;
#85876=CARTESIAN_POINT ( 'NONE',  ( -19.40337959798338119, 7.141409694766009508, -1.500000000000002220 ) ) ;
#85877=CARTESIAN_POINT ( 'NONE',  ( 7.679218611123722837, 20.28660689097963399, 11.49999999999999645 ) ) ;
#85879=DIRECTION ( 'NONE',  ( 1.000000000000000000, 3.773278334444166432E-23, 8.201307841325785021E-29 ) ) ;
#85881=CARTESIAN_POINT ( 'NONE',  ( -13.11617634606977489, 18.14055439154125438, -1.500000000000002220 ) ) ;
#85882=CARTESIAN_POINT ( 'NONE',  ( -79.39179774623507058, -25.27874917451760695, 6.303983963574001592 ) ) ;
#85883=CARTESIAN_POINT ( 'NONE',  ( -120.6228709571500559, -24.91570333823100825, 8.075032458375558164 ) ) ;
#85886=CARTESIAN_POINT ( 'NONE',  ( -35.54979913294904037, -24.15602025860895452, 10.28564288303536856 ) ) ;
#85887=ORIENTED_EDGE ( 'NONE', *, *, #22624, .T. ) ;
#85892=CARTESIAN_POINT ( 'NONE',  ( 18.68757921870947669, -9.911485057863893999, -1.500000000000002220 ) ) ;
#85894=CARTESIAN_POINT ( 'NONE',  ( -50.62375377019235145, -25.00158670708910691, 2.256160236439223254 ) ) ;
#85895=CARTESIAN_POINT ( 'NONE',  ( 18.38516380405726736, -11.72527425286322611, 11.49999999999998934 ) ) ;
#85896=CARTESIAN_POINT ( 'NONE',  ( -60.52287095715006160, -23.47596703998600631, 11.44779298504228926 ) ) ;
#85898=DIRECTION ( 'NONE',  ( -3.773278334453079618E-23, 0.9999999999976377785, 2.173523156925979975E-06 ) ) ;
#85899=CARTESIAN_POINT ( 'NONE',  ( -75.58953762381673869, -25.00158670708909625, 2.256160236439167299 ) ) ;
#85900=CARTESIAN_POINT ( 'NONE',  ( 21.36706796925463792, 4.321743776461201669, -1.500000000000002220 ) ) ;
#85901=CARTESIAN_POINT ( 'NONE',  ( -30.57287095715005520, -25.29575059580470153, 5.560322743885222074 ) ) ;
#85902=ORIENTED_EDGE ( 'NONE', *, *, #8060, .F. ) ;
#85904=LINE ( 'NONE', #62578, #92948 ) ;
#85905=ORIENTED_EDGE ( 'NONE', *, *, #25265, .F. ) ;
#85909=ORIENTED_EDGE ( 'NONE', *, *, #57924, .T. ) ;
#85910=B_SPLINE_CURVE_WITH_KNOTS ( 'NONE', 3,
 ( #28195, #41938, #35318, #72881 ),
 .UNSPECIFIED., .F., .F.,
 ( 4, 4 ),
 ( 0.000000000000000000, 9.999999999998897304E-05 ),
 .UNSPECIFIED. ) ;
#85911=CARTESIAN_POINT ( 'NONE',  ( -47.62287095715004881, -29.50247984919015209, -1.443849546365058689 ) ) ;
#85912=AXIS2_PLACEMENT_3D ( 'NONE', #96584, #98065, #4744 ) ;
#85913=CARTESIAN_POINT ( 'NONE',  ( -124.6228709571500701, -24.66019654487200086, 8.947790411086121054 ) ) ;
#85914=CARTESIAN_POINT ( 'NONE',  ( 12.26186175617451113, -17.30295086655154080, 11.49999999999998934 ) ) ;
#85916=CARTESIAN_POINT ( 'NONE',  ( -130.5728709571500588, -23.56000036390797092, -1.497999999999531040 ) ) ;
#85917=EDGE_CURVE ( 'NONE', #60317, #80103, #55964, .T. ) ;
#85919=CARTESIAN_POINT ( 'NONE',  ( -128.6228709571500417, -23.47593901973091235, -1.443836447538995760 ) ) ;
#85921=CARTESIAN_POINT ( 'NONE',  ( 16.99290379607386114, -9.356058476803225332, 11.49999999999998934 ) ) ;
#85923=CARTESIAN_POINT ( 'NONE',  ( -69.34449053119547557, -25.26190598939342280, 6.145922818284793365 ) ) ;
#85926=CARTESIAN_POINT ( 'NONE',  ( -18.91883139384513157, -4.797682538509264738, 11.49999999999999645 ) ) ;
#85927=CARTESIAN_POINT ( 'NONE',  ( -42.52287095715005449, -24.64965694238575011, 8.947790433994205372 ) ) ;
#85929=ORIENTED_EDGE ( 'NONE', *, *, #7730, .F. ) ;
#85930=CARTESIAN_POINT ( 'NONE',  ( -58.62287095715004881, -24.64965695001468404, 8.947790433994185832 ) ) ;
#85931=CARTESIAN_POINT ( 'NONE',  ( -59.52287095715004739, -24.66019654487199375, 8.947790411086128159 ) ) ;
#85932=CARTESIAN_POINT ( 'NONE',  ( -57.62287095715004881, -29.50250243563736774, 8.947779886222145151 ) ) ;
#85934=CARTESIAN_POINT ( 'NONE',  ( 2.289404864003111051, -19.52285375609543294, -1.500000000000002220 ) ) ;
#85935=CARTESIAN_POINT ( 'NONE',  ( -41.23075053442405391, -25.31583700235511714, 4.755616837286789966 ) ) ;
#85936=ORIENTED_EDGE ( 'NONE', *, *, #37768, .F. ) ;
#85937=CARTESIAN_POINT ( 'NONE',  ( 20.07693369621832602, 7.961103810760662647, -1.500000000000002220 ) ) ;
#85939=CARTESIAN_POINT ( 'NONE',  ( -77.92287095715005307, -23.47593901973090169, -1.443836447538997536 ) ) ;
#85940=CARTESIAN_POINT ( 'NONE',  ( -46.62287095715004881, -23.47593901973091235, -1.443836447539009749 ) ) ;
#85942=B_SPLINE_CURVE_WITH_KNOTS ( 'NONE', 3,
 ( #39989, #1940, #70949, #1437 ),
 .UNSPECIFIED., .F., .F.,
 ( 4, 4 ),
 ( 0.000000000000000000, 1.000000000000000000 ),
 .UNSPECIFIED. ) ;
#85944=CARTESIAN_POINT ( 'NONE',  ( -126.9228709571500247, -23.47593901973090524, -1.443836447538996204 ) ) ;
#85946=CARTESIAN_POINT ( 'NONE',  ( -126.5895376238166961, -23.48783264082479505, -1.443836473390057051 ) ) ;
#85947=CARTESIAN_POINT ( 'NONE',  ( -101.3308234756344035, -25.09314650408467173, 7.321823265739929809 ) ) ;
#85948=CARTESIAN_POINT ( 'NONE',  ( -109.3646363756176783, -25.27084415602777767, 4.082054875553674300 ) ) ;
#85949=CARTESIAN_POINT ( 'NONE',  ( -129.5218490263226272, -24.51314013834316796, 0.6176544820404223923 ) ) ;
#85950=CARTESIAN_POINT ( 'NONE',  ( -114.5158143349167403, -24.51419770103158768, 9.386484678747160970 ) ) ;
#85951=CARTESIAN_POINT ( 'NONE',  ( -13.91458393394894166, 14.26456941660895339, -1.500000000000002220 ) ) ;
#85953=CARTESIAN_POINT ( 'NONE',  ( -17.91562471463183570, -8.470225615102204841, -1.500000000000002220 ) ) ;
#85955=CARTESIAN_POINT ( 'NONE',  ( -51.62287095715005592, -24.66019654487199020, 8.947790411086135265 ) ) ;
#85956=CARTESIAN_POINT ( 'NONE',  ( -35.62287095715007723, -24.62285846362215125, 9.038163152653519106 ) ) ;
#85957=CARTESIAN_POINT ( 'NONE',  ( 19.63682106917175929, 6.691539877478525966, 11.49999999999999645 ) ) ;
#85958=DIRECTION ( 'NONE',  ( -3.773278334453080206E-23, 0.9999999999976377785, 2.173523156925979975E-06 ) ) ;
#85960=VECTOR ( 'NONE', #52081, 1000.000000000000114 ) ;
#85961=CARTESIAN_POINT ( 'NONE',  ( -106.5861045487569356, -24.65952944569304250, 1.056160979905701902 ) ) ;
#85962=CARTESIAN_POINT ( 'NONE',  ( 22.46337926046256328, 3.617889471270266277, 11.49999999999999645 ) ) ;
#85963=VERTEX_POINT ( 'NONE', #88946 ) ;
#85966=EDGE_LOOP ( 'NONE', ( #36683, #44165, #7853, #49476 ) ) ;
#85967=CARTESIAN_POINT ( 'NONE',  ( -16.64171244834553676, 11.49637152377623828, -1.500000000000002220 ) ) ;
#85968=DIRECTION ( 'NONE',  ( -3.773278334453079618E-23, 0.9999999999976377785, 2.173523156925979975E-06 ) ) ;
#85969=LINE ( 'NONE', #16955, #48000 ) ;
#85972=CARTESIAN_POINT ( 'NONE',  ( -109.5228709571500616, -29.50250243563736774, 8.947779886222136270 ) ) ;
#85973=CARTESIAN_POINT ( 'NONE',  ( -4.681240387505234857, -22.43558246840685300, 11.49999999999998934 ) ) ;
#85974=DIRECTION ( 'NONE',  ( 0.000000000000000000, -2.173523156925980399E-06, 0.9999999999976378895 ) ) ;
#85976=CARTESIAN_POINT ( 'NONE',  ( -2.642555958445479192, -21.45212208726272607, -1.500000000000002220 ) ) ;
#85977=EDGE_CURVE ( 'NONE', #44036, #20176, #42783, .T. ) ;
#85978=CARTESIAN_POINT ( 'NONE',  ( -9.893913718187896222, 18.50344063021147889, 11.49999999999999645 ) ) ;
#85979=ORIENTED_EDGE ( 'NONE', *, *, #68919, .F. ) ;
#85980=PLANE ( 'NONE',  #12965 ) ;
#85981=CARTESIAN_POINT ( 'NONE',  ( -124.6234875072562289, -24.65952944569305316, 1.056160979905708563 ) ) ;
#85982=CARTESIAN_POINT ( 'NONE',  ( 2.156995527713877259, 21.93451973775924557, -1.500000000000002220 ) ) ;
#85985=CARTESIAN_POINT ( 'NONE',  ( -102.5228709571500900, -23.47593901973090524, -1.443836447538996648 ) ) ;
#85986=ORIENTED_EDGE ( 'NONE', *, *, #62047, .F. ) ;
#85989=ORIENTED_EDGE ( 'NONE', *, *, #4984, .F. ) ;
#85990=CARTESIAN_POINT ( 'NONE',  ( -123.6228709571500133, -24.33927499327853994, 9.819080762295818943 ) ) ;
#85994=CARTESIAN_POINT ( 'NONE',  ( -83.52287095715009002, -23.95044443724993144, 10.65354141964648882 ) ) ;
#85995=CARTESIAN_POINT ( 'NONE',  ( -36.49756682744079228, -24.15543982623906771, -0.2315651400026672579 ) ) ;
#85996=EDGE_CURVE ( 'NONE', #36722, #47188, #62071, .T. ) ;
#85997=CARTESIAN_POINT ( 'NONE',  ( 17.04084431845542369, 11.38269047019995206, -1.500000000000002220 ) ) ;
#85998=ORIENTED_EDGE ( 'NONE', *, *, #13019, .T. ) ;
#85999=CARTESIAN_POINT ( 'NONE',  ( -61.52287095715006160, -23.47596703998600631, 11.44779298504228926 ) ) ;
#86001=CARTESIAN_POINT ( 'NONE',  ( -32.07722060962682775, -25.12026506542016335, 2.831122744435439209 ) ) ;
#86002=CARTESIAN_POINT ( 'NONE',  ( 18.42719714020066846, 12.55551944762973626, 11.49999999999998934 ) ) ;
#86003=CARTESIAN_POINT ( 'NONE',  ( -81.62287095715002749, -24.33832256526968862, 0.1851278514119888696 ) ) ;
#86004=CARTESIAN_POINT ( 'NONE',  ( -90.52287095715006160, -24.99156044556202616, 7.747789690856173195 ) ) ;
#86008=CARTESIAN_POINT ( 'NONE',  ( -14.03827505669662479, 15.38897104800697591, 11.49999999999998934 ) ) ;
#86010=CARTESIAN_POINT ( 'NONE',  ( -52.52287095715006160, -24.34917612407042142, 0.1852690917480152855 ) ) ;
#86011=ORIENTED_EDGE ( 'NONE', *, *, #13538, .T. ) ;
#86013=CARTESIAN_POINT ( 'NONE',  ( -51.38881019666819583, -25.25854471556175795, 6.651362266542584223 ) ) ;
#86014=CARTESIAN_POINT ( 'NONE',  ( 5.724939850241691275, 20.19279902153374096, -1.500000000000002220 ) ) ;
#86015=ORIENTED_EDGE ( 'NONE', *, *, #94194, .F. ) ;
#86017=CARTESIAN_POINT ( 'NONE',  ( -37.52287095715006870, -24.64965694238406613, 8.947790433994205372 ) ) ;
#86019=B_SPLINE_CURVE_WITH_KNOTS ( 'NONE', 3,
 ( #88903, #65585, #88399, #10774, #57466, #65089 ),
 .UNSPECIFIED., .F., .F.,
 ( 4, 2, 4 ),
 ( 0.000000000000000000, 0.001380764517853255106, 0.002761529035706510211 ),
 .UNSPECIFIED. ) ;
#86020=CARTESIAN_POINT ( 'NONE',  ( -119.6228709571500559, -23.47596703998600631, 11.44779298504227860 ) ) ;
#86021=CARTESIAN_POINT ( 'NONE',  ( -59.63756427278922700, -24.15543982623906416, -0.2315651400026668416 ) ) ;
#86022=CARTESIAN_POINT ( 'NONE',  ( -65.62287095715008434, -24.92604778743017846, 8.074972756849355449 ) ) ;
#86023=CARTESIAN_POINT ( 'NONE',  ( 21.93305185196877360, -3.456643806985262302, 11.49999999999999645 ) ) ;
#86024=VERTEX_POINT ( 'NONE', #81828 ) ;
#86025=CARTESIAN_POINT ( 'NONE',  ( -99.16166289166532977, -25.31166538673566180, 5.311370725864150266 ) ) ;
#86028=CARTESIAN_POINT ( 'NONE',  ( -21.16080155796574047, 8.166215375980355518, 11.49999999999998934 ) ) ;
#86030=EDGE_LOOP ( 'NONE', ( #84656, #23709, #20432, #57221 ) ) ;
#86032=ORIENTED_EDGE ( 'NONE', *, *, #6420, .T. ) ;
#86035=EDGE_CURVE ( 'NONE', #90963, #82927, #37798, .T. ) ;
#86036=CARTESIAN_POINT ( 'NONE',  ( -7.946508460909448956, -18.53024980520100939, -1.500000000000002220 ) ) ;
#86037=CARTESIAN_POINT ( 'NONE',  ( -88.55620429048340725, -23.48783264082478794, -1.443836473390064157 ) ) ;
#86040=CARTESIAN_POINT ( 'NONE',  ( -7.019573500991415749, 21.25910006591672996, -1.500000000000002220 ) ) ;
#86042=VERTEX_POINT ( 'NONE', #20911 ) ;
#86044=CARTESIAN_POINT ( 'NONE',  ( -101.5363578631102541, -25.25341111464364019, 6.270899391521124855 ) ) ;
#86045=CARTESIAN_POINT ( 'NONE',  ( -119.6228709571500559, -23.47596703998600631, 11.44779298504227860 ) ) ;
#86046=CARTESIAN_POINT ( 'NONE',  ( -73.62287095715005592, -24.65952944569304606, 1.056160979905698794 ) ) ;
#86047=CARTESIAN_POINT ( 'NONE',  ( -116.5228709571500616, -23.72773821059537269, 11.05748984161097503 ) ) ;
#86048=FACE_BOUND ( 'NONE', #20209, .T. ) ;
#86050=CARTESIAN_POINT ( 'NONE',  ( -18.73025074496528219, 5.678645368852136777, 11.49999999999998934 ) ) ;
#86053=CARTESIAN_POINT ( 'NONE',  ( 20.53733210929814845, -6.371126427052321795, -1.500000000000002220 ) ) ;
#86055=B_SPLINE_CURVE_WITH_KNOTS ( 'NONE', 3,
 ( #41853, #72793, #81398, #11879, #2288, #33218 ),
 .UNSPECIFIED., .F., .F.,
 ( 4, 2, 4 ),
 ( 1.570755371633954459E-05, 0.001396183895866085585, 0.002776660238015831676 ),
 .UNSPECIFIED. ) ;
#86057=CARTESIAN_POINT ( 'NONE',  ( -113.5228709571500616, -23.48786465467242479, 11.44779295918253936 ) ) ;
#86058=CARTESIAN_POINT ( 'NONE',  ( -30.57287095715006231, -29.50247984919009170, -1.443849575687677245 ) ) ;
#86059=CARTESIAN_POINT ( 'NONE',  ( -13.69284064830502423, 18.33895024417757469, -1.500000000000002220 ) ) ;
#86062=CARTESIAN_POINT ( 'NONE',  ( -124.5895376238167103, -24.64965694238408034, 8.947790433994649462 ) ) ;
#86064=CARTESIAN_POINT ( 'NONE',  ( 15.05167116458888010, 13.23127732593390959, 11.49999999999999645 ) ) ;
#86065=CARTESIAN_POINT ( 'NONE',  ( -79.55512035851637620, -25.26612423904884608, 4.736590108043814418 ) ) ;
#86068=CARTESIAN_POINT ( 'NONE',  ( -38.58953762381672448, -24.64965694238406613, 8.947790433994660120 ) ) ;
#86071=CARTESIAN_POINT ( 'NONE',  ( -21.74948284930419717, -1.071797830193938372, -1.500000000000002220 ) ) ;
#86072=EDGE_CURVE ( 'NONE', #51831, #55337, #46241, .T. ) ;
#86073=CARTESIAN_POINT ( 'NONE',  ( -45.52287095715006160, -23.48786465467240347, 11.44779295918255002 ) ) ;
#86074=CARTESIAN_POINT ( 'NONE',  ( -13.08164486973500118, 14.69858247433046650, -1.500000000000002220 ) ) ;
#86075=FACE_OUTER_BOUND ( 'NONE', #26006, .T. ) ;
#86076=DIRECTION ( 'NONE',  ( -3.773278334444166432E-23, 1.000000000000000000, 0.000000000000000000 ) ) ;
#86078=CARTESIAN_POINT ( 'NONE',  ( -73.62287095715005592, -23.48786465467241058, 11.44779295918254469 ) ) ;
#86079=CARTESIAN_POINT ( 'NONE',  ( -14.18348626307465743, -14.89297910716571849, 11.49999999999999645 ) ) ;
#86082=CARTESIAN_POINT ( 'NONE',  ( 21.37280783159109276, 7.349196219051140844, 11.49999999999999645 ) ) ;
#86085=DIRECTION ( 'NONE',  ( -3.773278334453080206E-23, 0.9999999999976377785, 2.173523156925979975E-06 ) ) ;
#86086=CARTESIAN_POINT ( 'NONE',  ( -26.45415226839903866, -24.86235341855187286, 6.807275991248984859 ) ) ;
#86087=CARTESIAN_POINT ( 'NONE',  ( -108.5895376238167387, -23.48783264082478794, -1.443836473390060604 ) ) ;
#86090=B_SPLINE_CURVE_WITH_KNOTS ( 'NONE', 3,
 ( #37002, #67967, #90291, #84167, #91289, #45622 ),
 .UNSPECIFIED., .F., .F.,
 ( 4, 2, 4 ),
 ( 0.000000000000000000, 0.001380901958385389412, 0.002761803916770778824 ),
 .UNSPECIFIED. ) ;
#86091=DIRECTION ( 'NONE',  ( 1.000000000000000000, 3.773278334444166432E-23, 8.201307841325785021E-29 ) ) ;
#86093=B_SPLINE_CURVE_WITH_KNOTS ( 'NONE', 3,
 ( #28115, #4778, #3791, #58569 ),
 .UNSPECIFIED., .F., .F.,
 ( 4, 4 ),
 ( 0.000000000000000000, 9.999999999998897304E-05 ),
 .UNSPECIFIED. ) ;
#86094=ORIENTED_EDGE ( 'NONE', *, *, #88092, .F. ) ;
#86095=CARTESIAN_POINT ( 'NONE',  ( 22.94779996701378266, 2.684060219229261968, 11.49999999999999645 ) ) ;
#86096=CARTESIAN_POINT ( 'NONE',  ( 20.43669262517703800, -10.12641136740851699, -1.500000000000002220 ) ) ;
#86097=CARTESIAN_POINT ( 'NONE',  ( -74.58444882624816330, -24.51314013834315375, 0.6176544820404124003 ) ) ;
#86099=CARTESIAN_POINT ( 'NONE',  ( -71.62287095715005592, -29.50247984919015209, -1.443849546365055359 ) ) ;
#86100=CARTESIAN_POINT ( 'NONE',  ( 18.93296920960566965, -11.98514031388154599, 11.49999999999999645 ) ) ;
#86103=AXIS2_PLACEMENT_3D ( 'NONE', #13547, #44516, #99285 ) ;
#86104=CARTESIAN_POINT ( 'NONE',  ( 18.54397492014093984, 11.73900455106235086, -1.500000000000002220 ) ) ;
#86106=DIRECTION ( 'NONE',  ( 1.000000000000000000, 3.773278334444167020E-23, 8.201307838832447938E-29 ) ) ;
#86107=CARTESIAN_POINT ( 'NONE',  ( -34.56115400525960979, -23.73791477778911485, 11.05961554403171299 ) ) ;
#86108=FACE_OUTER_BOUND ( 'NONE', #87746, .T. ) ;
#86110=CARTESIAN_POINT ( 'NONE',  ( -48.48461591879575394, -24.66019654487199730, 8.947790411086119278 ) ) ;
#86111=PLANE ( 'NONE',  #43009 ) ;
#86112=ORIENTED_EDGE ( 'NONE', *, *, #47191, .T. ) ;
#86113=CARTESIAN_POINT ( 'NONE',  ( -8.751980504941329286, -18.49744413911281882, -1.500000000000002220 ) ) ;
#86116=EDGE_LOOP ( 'NONE', ( #76641, #47339, #50572, #78505 ) ) ;
#86117=ORIENTED_EDGE ( 'NONE', *, *, #62652, .T. ) ;
#86119=CARTESIAN_POINT ( 'NONE',  ( -10.12245940999746985, -20.73198382670940987, -1.500000000000002220 ) ) ;
#86120=CARTESIAN_POINT ( 'NONE',  ( -40.11625432859197815, -25.26871255744266875, 3.880430150159563940 ) ) ;
#86122=CARTESIAN_POINT ( 'NONE',  ( 20.23811035156253979, -1.552196809741442696, -1.500000000000002220 ) ) ;
#86123=EDGE_LOOP ( 'NONE', ( #39837, #59217, #24109, #77062 ) ) ;
#86125=LINE ( 'NONE', #87124, #90341 ) ;
#86126=VECTOR ( 'NONE', #42052, 1000.000000000000114 ) ;
#86127=CARTESIAN_POINT ( 'NONE',  ( -93.62287095715008434, -24.50321055353803601, 9.387540953477522265 ) ) ;
#86129=CARTESIAN_POINT ( 'NONE',  ( 18.54456287915894563, -10.88813254144886322, 11.49999999999999645 ) ) ;
#86130=VERTEX_POINT ( 'NONE', #60994 ) ;
#86131=CARTESIAN_POINT ( 'NONE',  ( -89.62287095715004170, -24.64965695001468404, 8.947790433994180503 ) ) ;
#86132=PLANE ( 'NONE',  #476 ) ;
#86135=CARTESIAN_POINT ( 'NONE',  ( 20.64725891757762355, 2.036748910689437864, 11.49999999999998934 ) ) ;
#86137=CARTESIAN_POINT ( 'NONE',  ( -125.6251159883579902, -24.15503026093915295, -0.2815557561904348804 ) ) ;
#86139=CARTESIAN_POINT ( 'NONE',  ( -41.50559876260985703, -23.96169478059712787, 10.65365249895718591 ) ) ;
#86140=LINE ( 'NONE', #32352, #34060 ) ;
#86142=VERTEX_POINT ( 'NONE', #60507 ) ;
#86143=CARTESIAN_POINT ( 'NONE',  ( -49.21454750704995007, -25.12863070112381791, 7.069183623698430452 ) ) ;
#86145=CARTESIAN_POINT ( 'NONE',  ( -43.52945059456417454, -24.66019654487199375, 8.947790411086122830 ) ) ;
#86146=CARTESIAN_POINT ( 'NONE',  ( 16.78392297789021015, 14.29496084597832883, 11.49999999999999645 ) ) ;
#86147=B_SPLINE_CURVE_WITH_KNOTS ( 'NONE', 3,
 ( #32143, #7304, #45888, #23516 ),
 .UNSPECIFIED., .F., .F.,
 ( 4, 4 ),
 ( 0.000000000000000000, 9.999999999998897304E-05 ),
 .UNSPECIFIED. ) ;
#86148=CARTESIAN_POINT ( 'NONE',  ( -89.63827055049355863, -23.73791477778911840, 11.05961554403170233 ) ) ;
#86149=CARTESIAN_POINT ( 'NONE',  ( 2.010693963185784749, 22.50221635003889276, -1.500000000000002220 ) ) ;
#86150=CARTESIAN_POINT ( 'NONE',  ( -11.62490142266122639, -17.50836435561060256, -1.500000000000002220 ) ) ;
#86151=CARTESIAN_POINT ( 'NONE',  ( -100.6814946224345988, -25.30604030395771531, 4.890060448994407061 ) ) ;
#86153=EDGE_LOOP ( 'NONE', ( #25298, #55338, #9914, #9612 ) ) ;
#86159=ORIENTED_EDGE ( 'NONE', *, *, #11527, .F. ) ;
#86160=CARTESIAN_POINT ( 'NONE',  ( 6.139388171429570384, 20.22809724653347985, -1.500000000000002220 ) ) ;
#86161=CARTESIAN_POINT ( 'NONE',  ( -66.62287095715005592, -23.47596703998600276, 11.44779298504227683 ) ) ;
#86162=FACE_OUTER_BOUND ( 'NONE', #99138, .T. ) ;
#86163=CARTESIAN_POINT ( 'NONE',  ( -121.6267039608711400, -23.73766607897670156, -1.055555164236450905 ) ) ;
#86164=CARTESIAN_POINT ( 'NONE',  ( -109.5562042904833788, -24.66019654487200086, 8.947790411086124607 ) ) ;
#86166=CARTESIAN_POINT ( 'NONE',  ( 12.24756355222007898, 18.56953561607567238, -1.500000000000002220 ) ) ;
#86167=CARTESIAN_POINT ( 'NONE',  ( -49.32147450118114307, -25.13941415244942945, 7.186702086172223503 ) ) ;
#86168=ORIENTED_EDGE ( 'NONE', *, *, #97665, .T. ) ;
#86170=CARTESIAN_POINT ( 'NONE',  ( -37.64193424478225580, -24.15543982623907127, -0.2315651400026566831 ) ) ;
#86171=CARTESIAN_POINT ( 'NONE',  ( -126.5566007190337956, -23.48783264082477018, -1.443836473390087249 ) ) ;
#86173=CARTESIAN_POINT ( 'NONE',  ( -39.52287095715006870, -24.64965694238406613, 8.947790433994205372 ) ) ;
#86174=B_SPLINE_CURVE_WITH_KNOTS ( 'NONE', 3,
 ( #70194, #39237, #40746, #85919 ),
 .UNSPECIFIED., .F., .F.,
 ( 4, 4 ),
 ( 0.000000000000000000, 1.000000000000000000 ),
 .UNSPECIFIED. ) ;
#86175=CARTESIAN_POINT ( 'NONE',  ( 12.63578256557813795, 14.83599306707809085, -1.500000000000002220 ) ) ;
#86176=B_SPLINE_CURVE_WITH_KNOTS ( 'NONE', 3,
 ( #37583, #30965, #77127, #22 ),
 .UNSPECIFIED., .F., .F.,
 ( 4, 4 ),
 ( 0.9094323928107194144, 0.9104331398514848850 ),
 .UNSPECIFIED. ) ;
#86177=CARTESIAN_POINT ( 'NONE',  ( -21.38522110535750542, 1.317000383210971792, 11.49999999999998934 ) ) ;
#86179=CARTESIAN_POINT ( 'NONE',  ( -60.52841940773001284, -25.00182538069856619, 7.747789668514392325 ) ) ;
#86180=VECTOR ( 'NONE', #98929, 1000.000000000000114 ) ;
#86181=CARTESIAN_POINT ( 'NONE',  ( -100.6228709571500843, -24.92604778743017846, 8.074972756849359001 ) ) ;
#86182=FACE_OUTER_BOUND ( 'NONE', #81407, .T. ) ;
#86183=CARTESIAN_POINT ( 'NONE',  ( 22.03932947713327906, 5.445304565557160359, -1.500000000000002220 ) ) ;
#86184=ADVANCED_FACE ( 'NONE', ( #46767 ), #23396, .F. ) ;
#86187=CARTESIAN_POINT ( 'NONE',  ( -72.62287095715005592, -23.47593901973091235, -1.443836447539006196 ) ) ;
#86188=CARTESIAN_POINT ( 'NONE',  ( -9.044204435542846809, 17.70297415775587169, 11.49999999999999645 ) ) ;
#86189=CARTESIAN_POINT ( 'NONE',  ( -118.6228709571500701, -23.47596703998600631, 11.44779298504227683 ) ) ;
#86190=CARTESIAN_POINT ( 'NONE',  ( -89.81226385320381667, -25.18330262851202050, 6.757888827294434186 ) ) ;
#86191=DIRECTION ( 'NONE',  ( 0.5709972981045763341, 1.784358049357977499E-06, -0.8209519386383650197 ) ) ;
#86194=CARTESIAN_POINT ( 'NONE',  ( -58.52287095715009713, -24.66019654487199730, 8.947790411086121054 ) ) ;
#86195=CARTESIAN_POINT ( 'NONE',  ( -51.69439593370608321, -25.27412447326236489, 3.842802143524250091 ) ) ;
#86196=CARTESIAN_POINT ( 'NONE',  ( -2.787017431591729988, -21.48445716988565835, 11.49999999999998934 ) ) ;
#86198=CARTESIAN_POINT ( 'NONE',  ( -56.54231419305688888, -24.35071581493543391, 9.817618358456030592 ) ) ;
#86199=CARTESIAN_POINT ( 'NONE',  ( -18.70048401425367501, 5.426029767813830063, -1.500000000000002220 ) ) ;
#86201=CARTESIAN_POINT ( 'NONE',  ( -55.62855437941350090, -24.83644354573578283, 8.397322867130093016 ) ) ;
#86203=ORIENTED_EDGE ( 'NONE', *, *, #71358, .T. ) ;
#86205=ADVANCED_FACE ( 'NONE', ( #45269 ), #61993, .T. ) ;
#86206=CARTESIAN_POINT ( 'NONE',  ( -2.495337616714382367, -20.20711602426958819, 11.49999999999999645 ) ) ;
#86207=FACE_OUTER_BOUND ( 'NONE', #87933, .T. ) ;
#86210=CARTESIAN_POINT ( 'NONE',  ( -0.1182468871973336583, -21.51920112203868740, 11.01174216661999949 ) ) ;
#86211=CARTESIAN_POINT ( 'NONE',  ( -95.52287095715006160, -23.47596703998600631, 11.44779298504228215 ) ) ;
#86212=CARTESIAN_POINT ( 'NONE',  ( -96.62287095715007013, -23.95044443724992433, 10.65354141964649592 ) ) ;
#86214=CARTESIAN_POINT ( 'NONE',  ( -89.81226385320383088, -29.50249591506787894, 5.947779886229223045 ) ) ;
#86215=CARTESIAN_POINT ( 'NONE',  ( 17.77915467781788195, 9.360003092772107181, 11.49999999999998934 ) ) ;
#86216=EDGE_CURVE ( 'NONE', #17029, #83268, #87395, .T. ) ;
#86218=ORIENTED_EDGE ( 'NONE', *, *, #71690, .T. ) ;
#86220=CARTESIAN_POINT ( 'NONE',  ( -19.87571804785047647, -11.42512898079034400, 11.49999999999999645 ) ) ;
#86221=CARTESIAN_POINT ( 'NONE',  ( 9.518656604726816184, -20.62229310799655124, -1.500000000000002220 ) ) ;
#86222=ORIENTED_EDGE ( 'NONE', *, *, #5388, .T. ) ;
#86223=CARTESIAN_POINT ( 'NONE',  ( -30.47287095715006444, -25.24888046561066091, 6.123886400242147587 ) ) ;
#86225=FACE_OUTER_BOUND ( 'NONE', #16385, .T. ) ;
#86226=CARTESIAN_POINT ( 'NONE',  ( -30.57287095715006231, -25.11786545954479877, 2.750328999548155462 ) ) ;
#86227=EDGE_CURVE ( 'NONE', #58432, #60030, #69243, .T. ) ;
#86228=CARTESIAN_POINT ( 'NONE',  ( -84.52287095715006160, -23.48786465467241769, 11.44779295918254469 ) ) ;
#86229=VECTOR ( 'NONE', #419, 1000.000000000000114 ) ;
#86231=CARTESIAN_POINT ( 'NONE',  ( -33.52287095715006160, -23.47596703998600631, 11.44779298504229459 ) ) ;
#86232=CARTESIAN_POINT ( 'NONE',  ( -99.09705801370142808, -25.25460571337453075, 5.399822423257166548 ) ) ;
#86233=ORIENTED_EDGE ( 'NONE', *, *, #28886, .T. ) ;
#86234=CARTESIAN_POINT ( 'NONE',  ( 20.11976772532220181, -3.360927329567881205, -1.500000000000002220 ) ) ;
#86236=CARTESIAN_POINT ( 'NONE',  ( 9.898807498884217182, 20.75630955806377287, 11.49999999999998934 ) ) ;
#86238=EDGE_CURVE ( 'NONE', #15126, #64588, #71776, .T. ) ;
#86239=ORIENTED_EDGE ( 'NONE', *, *, #17580, .F. ) ;
#86240=CARTESIAN_POINT ( 'NONE',  ( -108.5552593049708889, -23.96169478059714564, 10.65365249895716993 ) ) ;
#86241=EDGE_CURVE ( 'NONE', #64814, #96161, #20893, .T. ) ;
#86244=CARTESIAN_POINT ( 'NONE',  ( -12.43717309395686499, -17.31322327496724611, 11.49999999999999645 ) ) ;
#86247=ORIENTED_EDGE ( 'NONE', *, *, #4256, .T. ) ;
#86248=CARTESIAN_POINT ( 'NONE',  ( 2.725811458822067657, 22.07344620009914138, 11.49999999999998934 ) ) ;
#86250=CARTESIAN_POINT ( 'NONE',  ( 17.27521350410721368, -11.31798593588896829, 11.49999999999998934 ) ) ;
#86251=B_SPLINE_CURVE_WITH_KNOTS ( 'NONE', 3,
 ( #24004, #54972, #10794, #2194, #34140, #55985, #10290, #1687 ),
 .UNSPECIFIED., .F., .F.,
 ( 4, 2, 2, 4 ),
 ( 3.992453237073820429E-05, 0.003307229636718544714, 0.004940882188892447430, 0.006574534741066350579 ),
 .UNSPECIFIED. ) ;
#86255=CARTESIAN_POINT ( 'NONE',  ( -69.85540018123268169, -25.31392322340849432, 5.203679841770401104 ) ) ;
#86257=CARTESIAN_POINT ( 'NONE',  ( -112.5228709571500616, -23.47593901973090524, -1.443836447538996426 ) ) ;
#86259=CARTESIAN_POINT ( 'NONE',  ( -58.64947410562866281, -23.73791477778911840, 11.05961554403170766 ) ) ;
#86260=CARTESIAN_POINT ( 'NONE',  ( -11.44352472427880052, 17.46665840655709090, -1.500000000000002220 ) ) ;
#86261=CARTESIAN_POINT ( 'NONE',  ( 19.95399986947220583, -8.914707708046476498, 11.49999999999999645 ) ) ;
#86264=CARTESIAN_POINT ( 'NONE',  ( 17.87336509531889561, -13.68139028912531785, -1.500000000000002220 ) ) ;
#86265=CARTESIAN_POINT ( 'NONE',  ( -44.62287095715004881, -24.64898659630528854, 1.056161002820819261 ) ) ;
#86267=AXIS2_PLACEMENT_3D ( 'NONE', #10191, #54873, #72105 ) ;
#86269=ORIENTED_EDGE ( 'NONE', *, *, #13084, .T. ) ;
#86274=CARTESIAN_POINT ( 'NONE',  ( -19.34459864454321831, 9.218434461607088792, -1.500000000000002220 ) ) ;
#86275=CARTESIAN_POINT ( 'NONE',  ( -21.90463088927077706, -4.570550247397807908, 11.49999999999999645 ) ) ;
#86276=ORIENTED_EDGE ( 'NONE', *, *, #91461, .F. ) ;
#86277=CARTESIAN_POINT ( 'NONE',  ( 0.4554788648648982474, -21.05657754196055009, 11.49999999999998934 ) ) ;
#86278=CARTESIAN_POINT ( 'NONE',  ( -30.48114189052184031, -24.75335575484455219, 8.640462295247351321 ) ) ;
#86279=CARTESIAN_POINT ( 'NONE',  ( -18.20579941527595480, -8.200869797747142087, -1.500000000000002220 ) ) ;
#86280=PLANE ( 'NONE',  #24204 ) ;
#86281=CARTESIAN_POINT ( 'NONE',  ( -43.52287095715005449, -24.51387760970724017, 9.387446482453409402 ) ) ;
#86282=CARTESIAN_POINT ( 'NONE',  ( -2.093881351098874521, -21.91542971883435698, -1.500000000000002220 ) ) ;
#86286=CARTESIAN_POINT ( 'NONE',  ( -72.52287095715007581, -29.50250243563736774, 8.947779886222143375 ) ) ;
#86288=CARTESIAN_POINT ( 'NONE',  ( 15.94631523246878579, 13.42178585792578360, 11.49999999999999645 ) ) ;
#86292=CARTESIAN_POINT ( 'NONE',  ( -19.99249555334884221, 7.427959064407942513, 11.49999999999998934 ) ) ;
#86293=DIRECTION ( 'NONE',  ( -3.773278334444166432E-23, 1.000000000000000000, 0.000000000000000000 ) ) ;
#86295=CARTESIAN_POINT ( 'NONE',  ( -109.9161100070499515, -25.06732983082694588, 7.447789526168954843 ) ) ;
#86297=CARTESIAN_POINT ( 'NONE',  ( 5.070899574700155732, -21.93562493352797915, -1.500000000000002220 ) ) ;
#86298=VECTOR ( 'NONE', #46996, 1000.000000000000114 ) ;
#86301=ORIENTED_EDGE ( 'NONE', *, *, #96714, .F. ) ;
#86305=CARTESIAN_POINT ( 'NONE',  ( -2.223759785643201869, -19.53228827767608777, 11.49999999999999645 ) ) ;
#86306=CARTESIAN_POINT ( 'NONE',  ( -49.52287095715004028, -23.94994826722564696, -0.6494450866342753592 ) ) ;
#86307=CARTESIAN_POINT ( 'NONE',  ( -32.52287095715004028, -24.35013146730201683, 9.818937971375111928 ) ) ;
#86309=ADVANCED_FACE ( 'NONE', ( #85311 ), #15802, .T. ) ;
#86310=CARTESIAN_POINT ( 'NONE',  ( -99.51176673733515088, -24.34968618360934300, 0.1864209137778966852 ) ) ;
#86311=CARTESIAN_POINT ( 'NONE',  ( -55.62287095715004170, -24.99132157543083821, 2.256160258750667502 ) ) ;
#86312=CARTESIAN_POINT ( 'NONE',  ( -124.5211384108013846, -23.96169478059714564, 10.65365249895717170 ) ) ;
#86314=EDGE_CURVE ( 'NONE', #89470, #62448, #48790, .T. ) ;
#86316=CARTESIAN_POINT ( 'NONE',  ( 3.912202881759007767, 19.34271161525698091, 11.49999999999998934 ) ) ;
#86317=ORIENTED_EDGE ( 'NONE', *, *, #33171, .T. ) ;
#86318=VECTOR ( 'NONE', #14796, 1000.000000000000114 ) ;
#86319=EDGE_CURVE ( 'NONE', #31094, #87031, #229, .T. ) ;
#86320=CARTESIAN_POINT ( 'NONE',  ( 12.43249465596513126, -15.92577207200969092, 11.49999999999999645 ) ) ;
#86322=B_SPLINE_CURVE_WITH_KNOTS ( 'NONE', 3,
 ( #66333, #19125, #65346, #64848, #42496, #57712 ),
 .UNSPECIFIED., .F., .F.,
 ( 4, 2, 4 ),
 ( 1.570887131794795405E-05, 0.001396322306279762808, 0.002776935741241577573 ),
 .UNSPECIFIED. ) ;
#86324=ORIENTED_EDGE ( 'NONE', *, *, #9471, .F. ) ;
#86325=CARTESIAN_POINT ( 'NONE',  ( -128.5228709571500758, -29.50250243563736774, 8.947779886222132717 ) ) ;
#86327=CARTESIAN_POINT ( 'NONE',  ( -50.92646440412053011, -25.30193528779874512, 5.303687469111972419 ) ) ;
#86330=PLANE ( 'NONE',  #41370 ) ;
#86331=CARTESIAN_POINT ( 'NONE',  ( -19.32702923155483177, -5.217993511516596961, -1.500000000000002220 ) ) ;
#86333=B_SPLINE_CURVE_WITH_KNOTS ( 'NONE', 3,
 ( #89922, #20391, #60489, #20895, #50375, #19404 ),
 .UNSPECIFIED., .F., .F.,
 ( 4, 2, 4 ),
 ( 0.000000000000000000, 0.001380901958385393966, 0.002761803916770787931 ),
 .UNSPECIFIED. ) ;
#86335=LINE ( 'NONE', #50654, #4729 ) ;
#86338=ADVANCED_FACE ( 'NONE', ( #97316 ), #54885, .F. ) ;
#86340=CARTESIAN_POINT ( 'NONE',  ( -92.52287095715006160, -24.64965694238407323, 8.947790433994196491 ) ) ;
#86341=CARTESIAN_POINT ( 'NONE',  ( -109.5174377349821953, -25.18430242849744261, 3.703579253892022471 ) ) ;
#86343=PLANE ( 'NONE',  #75930 ) ;
#86344=CARTESIAN_POINT ( 'NONE',  ( -41.26959558397307148, -25.08918874615346439, 7.338714959427068862 ) ) ;
#86348=AXIS2_PLACEMENT_3D ( 'NONE', #86696, #40540, #54766 ) ;
#86349=CARTESIAN_POINT ( 'NONE',  ( -99.90552080552691905, -25.31392319263090585, 5.203681702801228326 ) ) ;
#86351=CARTESIAN_POINT ( 'NONE',  ( -12.35269427871797987, -16.12754648828645543, -1.500000000000002220 ) ) ;
#86353=CARTESIAN_POINT ( 'NONE',  ( -109.5562042904833646, -23.48783264082478439, -1.443836473390060604 ) ) ;
#86354=CARTESIAN_POINT ( 'NONE',  ( -100.5228709571500616, -29.50248528299804818, 1.056150453629042030 ) ) ;
#86357=CARTESIAN_POINT ( 'NONE',  ( -94.62287095715005592, -23.47596703998600631, 11.44779298504227860 ) ) ;
#86358=CARTESIAN_POINT ( 'NONE',  ( -20.08517628505838815, -1.856936949192496300, -1.500000000000002220 ) ) ;
#86359=CARTESIAN_POINT ( 'NONE',  ( 3.428800225705347149, -20.88102749682517612, 11.49999999999999645 ) ) ;
#86360=CARTESIAN_POINT ( 'NONE',  ( 19.81268554055766273, 9.900562300003143079, -1.500000000000002220 ) ) ;
#86361=ADVANCED_FACE ( 'NONE', ( #81091 ), #78194, .T. ) ;
#86362=CARTESIAN_POINT ( 'NONE',  ( -10.41206725544052780, -17.73373708237225799, 11.49999999999998934 ) ) ;
#86364=ORIENTED_EDGE ( 'NONE', *, *, #85269, .F. ) ;
#86365=CARTESIAN_POINT ( 'NONE',  ( -43.52287095715006870, -24.50216790748204332, 0.6166512839542462876 ) ) ;
#86367=CARTESIAN_POINT ( 'NONE',  ( -88.58953762381669605, -24.64965694238575011, 8.947790433994194714 ) ) ;
#86369=VERTEX_POINT ( 'NONE', #8707 ) ;
#86370=VERTEX_POINT ( 'NONE', #33922 ) ;
#86371=EDGE_LOOP ( 'NONE', ( #91452, #79121, #57467, #77981 ) ) ;
#86372=FACE_OUTER_BOUND ( 'NONE', #93988, .T. ) ;
#86375=CARTESIAN_POINT ( 'NONE',  ( -2.856624844580134770, 20.53689577262001364, -1.500000000000002220 ) ) ;
#86376=CARTESIAN_POINT ( 'NONE',  ( -20.21959982808627032, -7.803091810188320210, 11.49999999999999645 ) ) ;
#86379=CARTESIAN_POINT ( 'NONE',  ( -46.58953762381671737, -24.64965694238406968, 8.947790433994658343 ) ) ;
#86380=CARTESIAN_POINT ( 'NONE',  ( -111.2237262587288598, -25.16193699626175118, 3.138289488163724439 ) ) ;
#86381=CARTESIAN_POINT ( 'NONE',  ( -21.90463088927077706, -4.570550247397807908, -1.500000000000002220 ) ) ;
#86382=CARTESIAN_POINT ( 'NONE',  ( -71.52287095715010423, -23.48783264082477018, -1.443836473390091246 ) ) ;
#86383=CARTESIAN_POINT ( 'NONE',  ( -84.58539173471375250, -24.51314013834316441, 0.6176544820404183955 ) ) ;
#86384=ORIENTED_EDGE ( 'NONE', *, *, #66085, .F. ) ;
#86385=B_SPLINE_CURVE_WITH_KNOTS ( 'NONE', 3,
 ( #19512, #44366, #73315, #67209 ),
 .UNSPECIFIED., .F., .F.,
 ( 4, 4 ),
 ( 0.7002859815557139767, 0.7092924128278295104 ),
 .UNSPECIFIED. ) ;
#86386=CARTESIAN_POINT ( 'NONE',  ( -119.4728709571500644, -25.40558663563398056, 5.000950440326719537 ) ) ;
#86387=CARTESIAN_POINT ( 'NONE',  ( -35.64141604588792944, -24.52399227489126687, 9.353111116836519301 ) ) ;
#86390=CARTESIAN_POINT ( 'NONE',  ( -102.5228709571500758, -29.50250243563736774, 8.947779886222138046 ) ) ;
#86391=EDGE_LOOP ( 'NONE', ( #93465, #4483, #2901, #30090 ) ) ;
#86392=CARTESIAN_POINT ( 'NONE',  ( -112.6228709571500559, -29.50250243563736774, 8.947779886222136270 ) ) ;
#86393=CARTESIAN_POINT ( 'NONE',  ( 17.87031378931267867, -11.31994873005049129, -1.500000000000002220 ) ) ;
#86394=ORIENTED_EDGE ( 'NONE', *, *, #61276, .T. ) ;
#86395=CARTESIAN_POINT ( 'NONE',  ( -50.62611295517817211, -24.92564183028979130, 1.928384488918255535 ) ) ;
#86396=CARTESIAN_POINT ( 'NONE',  ( -3.204121956075930200, -21.57847171274271858, -1.500000000000002220 ) ) ;
#86397=CARTESIAN_POINT ( 'NONE',  ( -90.62287095715004170, -29.50248789122583659, 2.256150453626215580 ) ) ;
#86398=CARTESIAN_POINT ( 'NONE',  ( -62.62287095715004881, -24.66019654487199020, 8.947790411086131712 ) ) ;
#86399=PLANE ( 'NONE',  #35193 ) ;
#86400=CARTESIAN_POINT ( 'NONE',  ( -11.04117723084791614, -18.81814233335528286, -1.500000000000002220 ) ) ;
#86401=CARTESIAN_POINT ( 'NONE',  ( -30.57287095715007297, -25.09900243522883301, 2.757825582299280764 ) ) ;
#86403=FACE_OUTER_BOUND ( 'NONE', #47673, .T. ) ;
#86404=CARTESIAN_POINT ( 'NONE',  ( -85.62828315695789172, -24.73531770709095312, 8.716586749053508498 ) ) ;
#86406=CARTESIAN_POINT ( 'NONE',  ( -129.5558062447522047, -24.35071581493544102, 9.817618358456021710 ) ) ;
#86407=VERTEX_POINT ( 'NONE', #4479 ) ;
#86409=EDGE_LOOP ( 'NONE', ( #86985, #63781, #71962, #28031 ) ) ;
#86410=CARTESIAN_POINT ( 'NONE',  ( -29.23542772204989859, -25.18830698421514924, 4.359319682132476004 ) ) ;
#86411=CARTESIAN_POINT ( 'NONE',  ( -82.55857439284859822, -23.73766607897671577, -1.055555164236435362 ) ) ;
#86412=CARTESIAN_POINT ( 'NONE',  ( 18.67678363807796416, 10.12720680154768971, 11.49999999999998934 ) ) ;
#86413=CARTESIAN_POINT ( 'NONE',  ( -125.5895376238167245, -23.47593901973091235, -1.443836447538995760 ) ) ;
#86414=CARTESIAN_POINT ( 'NONE',  ( -41.58953762381673158, -24.65952944569304250, 1.056160979905689024 ) ) ;
#86417=AXIS2_PLACEMENT_3D ( 'NONE', #13028, #90169, #61232 ) ;
#86418=CARTESIAN_POINT ( 'NONE',  ( 14.52268490272241408, 12.84546865777419455, -1.500000000000002220 ) ) ;
#86419=CARTESIAN_POINT ( 'NONE',  ( -45.49986917282443244, -24.15503026093915651, -0.2815557561904415418 ) ) ;
#86422=CARTESIAN_POINT ( 'NONE',  ( -8.292788067677484776, 17.68049324621676632, 11.49999999999999645 ) ) ;
#86424=ADVANCED_FACE ( 'NONE', ( #34421 ), #64401, .T. ) ;
#86428=CARTESIAN_POINT ( 'NONE',  ( -98.52287095715009002, -24.66019654487200441, 8.947790411086119278 ) ) ;
#86429=CARTESIAN_POINT ( 'NONE',  ( -75.62287095715004170, -24.15431212366389957, -0.2830839119429070516 ) ) ;
#86430=EDGE_CURVE ( 'NONE', #81257, #54341, #57283, .T. ) ;
#86433=CARTESIAN_POINT ( 'NONE',  ( -19.15055961920884542, -4.482958728538418924, -1.500000000000002220 ) ) ;
#86434=B_SPLINE_SURFACE_WITH_KNOTS ( 'NONE', 3, 3, ( 
 ( #44113, #37492, #67452, #52722 ),
 ( #22245, #98377, #28881, #75536 ),
 ( #30373, #22745, #83659, #59845 ),
 ( #29875, #38493, #98883, #21252 ),
 ( #13640, #69443, #51726, #29374 ),
 ( #100361, #61843, #60351, #84156 ),
 ( #84660, #76532, #44610, #20754 ) ),
 .UNSPECIFIED., .F., .F., .F.,
 ( 4, 3, 4 ),
 ( 4, 4 ),
 ( 0.7945040050992245861, 0.8970133687736503436, 0.9995227324480759901 ),
 ( 0.4696133325002398995, 0.4708428617326421151 ),
 .UNSPECIFIED. ) ;
#86436=CARTESIAN_POINT ( 'NONE',  ( -18.50814150397365410, 11.09706937414969374, 11.49999999999998934 ) ) ;
#86437=CARTESIAN_POINT ( 'NONE',  ( -97.58953762381675290, -23.47596703998600631, 11.44779298504227683 ) ) ;
#86439=CARTESIAN_POINT ( 'NONE',  ( 16.03631736716203449, -16.64276770305488284, -1.500000000000002220 ) ) ;
#86442=CARTESIAN_POINT ( 'NONE',  ( -103.6228709571500559, -29.50250243563736774, 8.947779886222138046 ) ) ;
#86443=CARTESIAN_POINT ( 'NONE',  ( -126.6228709571500275, -23.48783264082479505, -1.443836473390057051 ) ) ;
#86445=CARTESIAN_POINT ( 'NONE',  ( -111.7494854843401555, -25.10921632119354641, 4.020187994209829974 ) ) ;
#86446=DIRECTION ( 'NONE',  ( 0.000000000000000000, -2.173523156925979552E-06, 0.9999999999976378895 ) ) ;
#86447=CARTESIAN_POINT ( 'NONE',  ( -114.5904428896033522, -24.15620529776629155, 10.23563542870659404 ) ) ;
#86448=CARTESIAN_POINT ( 'NONE',  ( -15.73602684802347440, -12.20685706852216867, -1.500000000000002220 ) ) ;
#86449=AXIS2_PLACEMENT_3D ( 'NONE', #51349, #27012, #66602 ) ;
#86450=CARTESIAN_POINT ( 'NONE',  ( -75.63150933904543649, -24.63419186844611275, 9.035850630976923981 ) ) ;
#86451=CARTESIAN_POINT ( 'NONE',  ( 19.75055111929153639, -1.948201398878238066, -1.500000000000002220 ) ) ;
#86452=ORIENTED_EDGE ( 'NONE', *, *, #95999, .F. ) ;
#86454=VECTOR ( 'NONE', #35335, 1000.000000000000114 ) ;
#86457=CARTESIAN_POINT ( 'NONE',  ( -1.843323519027639357, -20.62917239659568835, 11.49999999999999645 ) ) ;
#86459=CARTESIAN_POINT ( 'NONE',  ( -106.5500360596543317, -24.51314013834316441, 0.6176544820404206160 ) ) ;
#86460=CARTESIAN_POINT ( 'NONE',  ( -9.230423729802735622, -20.81519635545753033, 11.49999999999999645 ) ) ;
#86461=ORIENTED_EDGE ( 'NONE', *, *, #62098, .F. ) ;
#86462=CARTESIAN_POINT ( 'NONE',  ( -69.51085230579893448, -23.96119346886880663, -0.6495511937832122440 ) ) ;
#86463=CARTESIAN_POINT ( 'NONE',  ( -100.5562042904834072, -25.00158670708909625, 2.256160236439166411 ) ) ;
#86464=ORIENTED_EDGE ( 'NONE', *, *, #14244, .T. ) ;
#86465=CARTESIAN_POINT ( 'NONE',  ( -5.148175472751820081, -19.54457232503198227, 11.49999999999998934 ) ) ;
#86467=B_SPLINE_CURVE_WITH_KNOTS ( 'NONE', 3,
 ( #58176, #58666, #89120, #89614 ),
 .UNSPECIFIED., .F., .F.,
 ( 4, 4 ),
 ( 0.1688795826442255343, 0.1698803296849912270 ),
 .UNSPECIFIED. ) ;
#86469=EDGE_CURVE ( 'NONE', #97847, #19743, #50152, .T. ) ;
#86471=CARTESIAN_POINT ( 'NONE',  ( -40.62287095715005592, -23.48786465467240347, 11.44779295918255180 ) ) ;
#86472=CARTESIAN_POINT ( 'NONE',  ( 7.457602374657920308, -21.66695214233757838, 11.49999999999998934 ) ) ;
#86474=CARTESIAN_POINT ( 'NONE',  ( -19.63739455291241498, 3.909132673056371132, -1.500000000000002220 ) ) ;
#86475=CARTESIAN_POINT ( 'NONE',  ( -36.62287095715005592, -24.50321055353804667, 9.387540953477540029 ) ) ;
#86476=CARTESIAN_POINT ( 'NONE',  ( 20.89173079421859214, 1.537965369061287557, 11.49999999999999645 ) ) ;
#86477=CARTESIAN_POINT ( 'NONE',  ( -122.6228709571500417, -23.73934037231758154, 11.05740245334328264 ) ) ;
#86478=CARTESIAN_POINT ( 'NONE',  ( -124.5548839462270365, -24.34968618360934300, 0.1864209137778899961 ) ) ;
#86479=CARTESIAN_POINT ( 'NONE',  ( -5.411813039392390223, -21.34095290059367755, -1.500000000000002220 ) ) ;
#86480=EDGE_CURVE ( 'NONE', #89504, #39568, #75348, .T. ) ;
#86482=AXIS2_PLACEMENT_3D ( 'NONE', #69463, #67980, #53251 ) ;
#86483=VERTEX_POINT ( 'NONE', #5953 ) ;
#86485=ADVANCED_FACE ( 'NONE', ( #97804 ), #89707, .T. ) ;
#86490=VECTOR ( 'NONE', #51506, 1000.000000000000114 ) ;
#86491=VERTEX_POINT ( 'NONE', #27800 ) ;
#86493=CARTESIAN_POINT ( 'NONE',  ( -69.52287095715006160, -29.50247984919015209, -1.443849546365055359 ) ) ;
#86495=CARTESIAN_POINT ( 'NONE',  ( 13.18781518674367348, -15.76626393773247337, -1.500000000000002220 ) ) ;
#86496=ORIENTED_EDGE ( 'NONE', *, *, #42707, .T. ) ;
#86500=CARTESIAN_POINT ( 'NONE',  ( -17.00426676922356606, 14.40147940013276973, 11.49999999999998934 ) ) ;
#86501=DIRECTION ( 'NONE',  ( -3.773278334453079030E-23, 0.9999999999976377785, 2.173523156925979128E-06 ) ) ;
#86502=DIRECTION ( 'NONE',  ( 1.000000000000000000, 3.773278334444166432E-23, 8.201307841325785021E-29 ) ) ;
#86504=CARTESIAN_POINT ( 'NONE',  ( -96.62287095714999907, -24.51283580621364067, 0.6167428607019872500 ) ) ;
#86505=CARTESIAN_POINT ( 'NONE',  ( -124.6228709571500275, -23.72747288104469732, -1.053458166803224794 ) ) ;
#86506=CARTESIAN_POINT ( 'NONE',  ( -14.03827505669662479, 15.38897104800697591, -1.500000000000002220 ) ) ;
#86507=ORIENTED_EDGE ( 'NONE', *, *, #21233, .T. ) ;
#86510=ORIENTED_EDGE ( 'NONE', *, *, #79972, .T. ) ;
#86511=B_SPLINE_CURVE_WITH_KNOTS ( 'NONE', 3,
 ( #3836, #95174, #96667, #66247 ),
 .UNSPECIFIED., .F., .F.,
 ( 4, 4 ),
 ( 0.000000000000000000, 9.999999999998897304E-05 ),
 .UNSPECIFIED. ) ;
#86512=CARTESIAN_POINT ( 'NONE',  ( -103.6228709571500559, -23.47593901973091235, -1.443836447539001089 ) ) ;
#86513=CARTESIAN_POINT ( 'NONE',  ( -20.39251343623233836, 4.912230638944180328, -1.500000000000002220 ) ) ;
#86514=EDGE_LOOP ( 'NONE', ( #15310, #44891, #30466, #54872 ) ) ;
#86519=CARTESIAN_POINT ( 'NONE',  ( -59.65599814963717051, -23.48783264082476308, -1.443836473390097908 ) ) ;
#86521=CARTESIAN_POINT ( 'NONE',  ( -57.52287095715003318, -23.48783264082476663, -1.443836473390093911 ) ) ;
#86522=CARTESIAN_POINT ( 'NONE',  ( -18.24902840909259538, -12.68162010772806170, 11.49999999999999645 ) ) ;
#86523=ORIENTED_EDGE ( 'NONE', *, *, #17447, .T. ) ;
#86526=VERTEX_POINT ( 'NONE', #98800 ) ;
#86527=VECTOR ( 'NONE', #54176, 1000.000000000000114 ) ;
#86528=CARTESIAN_POINT ( 'NONE',  ( -7.311831771877058905, -21.45741656709679646, 11.49999999999998934 ) ) ;
#86529=EDGE_CURVE ( 'NONE', #92377, #53767, #17314, .T. ) ;
#86531=ORIENTED_EDGE ( 'NONE', *, *, #63940, .F. ) ;
#86533=ORIENTED_EDGE ( 'NONE', *, *, #53326, .T. ) ;
#86535=CARTESIAN_POINT ( 'NONE',  ( -6.497366621441947210, -19.08602653180391329, -1.500000000000002220 ) ) ;
#86537=ORIENTED_EDGE ( 'NONE', *, *, #1770, .T. ) ;
#86538=ADVANCED_FACE ( 'NONE', ( #13061 ), #67373, .T. ) ;
#86539=CARTESIAN_POINT ( 'NONE',  ( -55.62287095715004170, -29.50248789122583659, 2.256150453626215580 ) ) ;
#86540=CARTESIAN_POINT ( 'NONE',  ( 17.95543856985664277, -13.40637504462900331, -1.500000000000002220 ) ) ;
#86541=ORIENTED_EDGE ( 'NONE', *, *, #97089, .T. ) ;
#86543=CARTESIAN_POINT ( 'NONE',  ( -112.5150097671653810, -24.51419770103158413, 9.386484678747166299 ) ) ;
#86544=CARTESIAN_POINT ( 'NONE',  ( -94.55479201150613733, -23.96169478059713143, 10.65365249895717881 ) ) ;
#86549=CARTESIAN_POINT ( 'NONE',  ( -58.52287095715006160, -23.48786465467241058, 11.44779295918254824 ) ) ;
#86550=CARTESIAN_POINT ( 'NONE',  ( -19.37596289572233488, 2.755671585415585767, 11.49999999999998934 ) ) ;
#86554=CARTESIAN_POINT ( 'NONE',  ( 14.19067371521932230, 16.14321034643037578, 11.49999999999998934 ) ) ;
#86555=B_SPLINE_CURVE_WITH_KNOTS ( 'NONE', 3,
 ( #86968, #25065, #8346, #39294, #95089, #9342 ),
 .UNSPECIFIED., .F., .F.,
 ( 4, 2, 4 ),
 ( 6.384118678619663671E-06, 0.001386860460828381273, 0.002767336802978143193 ),
 .UNSPECIFIED. ) ;
#86556=CARTESIAN_POINT ( 'NONE',  ( -128.5896665593298849, -24.34968618360935011, 0.1864209137779018477 ) ) ;
#86558=CARTESIAN_POINT ( 'NONE',  ( -121.5228709571500332, -24.51283580621365488, 0.6167428607019768139 ) ) ;
#86559=LINE ( 'NONE', #7427, #68682 ) ;
#86560=CARTESIAN_POINT ( 'NONE',  ( -70.52287095715007581, -25.00182538069145366, 7.747789668545101094 ) ) ;
#86561=CARTESIAN_POINT ( 'NONE',  ( -8.048360580058307789, -21.46040670285860230, -1.500000000000002220 ) ) ;
#86564=LINE ( 'NONE', #87063, #26434 ) ;
#86565=CARTESIAN_POINT ( 'NONE',  ( 18.22975119132022215, -8.346483668847822557, 11.49999999999999645 ) ) ;
#86567=CARTESIAN_POINT ( 'NONE',  ( -57.55620429048338593, -24.66019654487199020, 8.947790411086131712 ) ) ;
#86570=ADVANCED_FACE ( 'NONE', ( #35912 ), #37418, .T. ) ;
#86572=CARTESIAN_POINT ( 'NONE',  ( 14.05712878599199200, -16.60762996970646199, -1.500000000000002220 ) ) ;
#86574=CARTESIAN_POINT ( 'NONE',  ( 0.6594449095415070294, 19.62168050102039629, -1.500000000000002220 ) ) ;
#86575=CARTESIAN_POINT ( 'NONE',  ( -85.52287095715006160, -24.63345952396255356, 9.038047939301506517 ) ) ;
#86576=CARTESIAN_POINT ( 'NONE',  ( -40.76736580419878919, -25.19037098555834575, 3.332599596532740183 ) ) ;
#86579=CARTESIAN_POINT ( 'NONE',  ( 11.80677006232881254, 16.86875346446678137, 11.49999999999999645 ) ) ;
#86580=FACE_OUTER_BOUND ( 'NONE', #6106, .T. ) ;
#86581=VECTOR ( 'NONE', #74480, 1000.000000000000114 ) ;
#86583=CARTESIAN_POINT ( 'NONE',  ( 7.090404290683943067, 21.45231405096426514, 11.49999999999999645 ) ) ;
#86585=CARTESIAN_POINT ( 'NONE',  ( -70.29041810236439858, -25.12219144531777459, 7.100646716122134272 ) ) ;
#86586=CARTESIAN_POINT ( 'NONE',  ( -27.30354941466529439, -24.79259182970212549, 7.548671802243905660 ) ) ;
#86587=CARTESIAN_POINT ( 'NONE',  ( -125.6234888013038926, -25.00182538069147498, 7.747789668545045139 ) ) ;
#86589=EDGE_CURVE ( 'NONE', #24503, #54649, #45532, .T. ) ;
#86590=LINE ( 'NONE', #46044, #100237 ) ;
#86591=VECTOR ( 'NONE', #31844, 1000.000000000000114 ) ;
#86592=LINE ( 'NONE', #95710, #23636 ) ;
#86594=VERTEX_POINT ( 'NONE', #37909 ) ;
#86595=CARTESIAN_POINT ( 'NONE',  ( 23.08992502549420323, -0.8469403905869224980, 11.49999999999999645 ) ) ;
#86596=CARTESIAN_POINT ( 'NONE',  ( 22.28265747778879202, 5.072132558558076099, 11.49999999999998934 ) ) ;
#86598=CARTESIAN_POINT ( 'NONE',  ( -96.58459391463640031, -24.65952944569305316, 1.056160979905706121 ) ) ;
#86599=CARTESIAN_POINT ( 'NONE',  ( -63.57960293449288258, -24.66019654487200086, 8.947790411086121054 ) ) ;
#86600=CARTESIAN_POINT ( 'NONE',  ( 19.77452139984142221, -10.64395493966388706, 11.49999999999999645 ) ) ;
#86602=DIRECTION ( 'NONE',  ( 1.000000000000000000, 3.773278334444166432E-23, 8.201307841325785021E-29 ) ) ;
#86603=CARTESIAN_POINT ( 'NONE',  ( -21.09739860443290382, 5.981408608369527258, -1.500000000000002220 ) ) ;
#86604=EDGE_CURVE ( 'NONE', #70027, #15603, #76452, .T. ) ;
#86605=DIRECTION ( 'NONE',  ( -3.773278334444166432E-23, 1.000000000000000000, 0.000000000000000000 ) ) ;
#86607=CARTESIAN_POINT ( 'NONE',  ( -110.6228709571500559, -25.00158670708909625, 2.256160236439165967 ) ) ;
#86609=ORIENTED_EDGE ( 'NONE', *, *, #84526, .F. ) ;
#86610=CARTESIAN_POINT ( 'NONE',  ( -48.56040166396459057, -23.73791477778911840, 11.05961554403170766 ) ) ;
#86611=ADVANCED_FACE ( 'NONE', ( #51646 ), #75252, .T. ) ;
#86612=DIRECTION ( 'NONE',  ( -1.000000000000000000, -3.773278334444167608E-23, -8.201307833595939069E-29 ) ) ;
#86614=CARTESIAN_POINT ( 'NONE',  ( -15.03541999946025243, -13.88573836563254460, -1.500000000000002220 ) ) ;
#86615=ORIENTED_EDGE ( 'NONE', *, *, #90243, .F. ) ;
#86616=EDGE_LOOP ( 'NONE', ( #13374, #95852, #58669, #9478 ) ) ;
#86619=CARTESIAN_POINT ( 'NONE',  ( 20.31487730549432413, -11.01532776123576518, -1.500000000000002220 ) ) ;
#86620=CARTESIAN_POINT ( 'NONE',  ( -77.62287095715005592, -29.50247984919015209, -1.443849546365053582 ) ) ;
#86621=CARTESIAN_POINT ( 'NONE',  ( 5.347689060783223702, 19.56899250667117229, -1.500000000000002220 ) ) ;
#86625=CARTESIAN_POINT ( 'NONE',  ( -72.52287095715007581, -24.33832256527048798, 0.1851278514138591791 ) ) ;
#86626=CARTESIAN_POINT ( 'NONE',  ( -101.4434582987268811, -25.22066056363861719, 6.520318706290999522 ) ) ;
#86627=CARTESIAN_POINT ( 'NONE',  ( -98.22287095715006444, -23.47596703998600276, 11.44779298504227683 ) ) ;
#86628=CARTESIAN_POINT ( 'NONE',  ( -8.581294335678165908, -19.67629172487136557, 11.49999999999999645 ) ) ;
#86629=ORIENTED_EDGE ( 'NONE', *, *, #40743, .F. ) ;
#86631=CARTESIAN_POINT ( 'NONE',  ( -49.46456330771200527, -25.26385804535316026, 4.758318182142605934 ) ) ;
#86632=AXIS2_PLACEMENT_3D ( 'NONE', #54141, #52132, #14046 ) ;
#86634=CARTESIAN_POINT ( 'NONE',  ( 14.12806351585482112, -15.20395780304818523, -1.500000000000002220 ) ) ;
#86637=LINE ( 'NONE', #71423, #71810 ) ;
#86639=CARTESIAN_POINT ( 'NONE',  ( -111.6235230997591685, -24.66019654487200441, 8.947790411086105067 ) ) ;
#86640=CARTESIAN_POINT ( 'NONE',  ( -102.6228709571500559, -23.47596703998600631, 11.44779298504227683 ) ) ;
#86641=EDGE_LOOP ( 'NONE', ( #45945, #59891, #99817, #51808 ) ) ;
#86642=ORIENTED_EDGE ( 'NONE', *, *, #40504, .F. ) ;
#86643=CARTESIAN_POINT ( 'NONE',  ( -28.58953762381671382, -24.50475509704323329, 8.947790423985489738 ) ) ;
#86645=CARTESIAN_POINT ( 'NONE',  ( -29.78642357706881683, -25.22946142887256826, 4.201050309516873860 ) ) ;
#86646=CARTESIAN_POINT ( 'NONE',  ( 3.837975233861466329, 21.70421690940786874, 11.49999999999999645 ) ) ;
#86647=ORIENTED_EDGE ( 'NONE', *, *, #88047, .T. ) ;
#86648=CARTESIAN_POINT ( 'NONE',  ( -103.5856513585207637, -24.65952944569304606, 1.056160979905703234 ) ) ;
#86649=CARTESIAN_POINT ( 'NONE',  ( 5.419076944403256491, 21.93356404788375258, 11.49999999999998934 ) ) ;
#86650=CARTESIAN_POINT ( 'NONE',  ( 14.98681507544721292, -14.71779577663021321, -1.500000000000002220 ) ) ;
#86651=CARTESIAN_POINT ( 'NONE',  ( -62.52287095715006160, -23.94994826722564696, -0.6494450866342735829 ) ) ;
#86653=ORIENTED_EDGE ( 'NONE', *, *, #14157, .F. ) ;
#86656=CARTESIAN_POINT ( 'NONE',  ( -90.62287095715001328, -24.51254535404253332, 9.355368623467651190 ) ) ;
#86657=ORIENTED_EDGE ( 'NONE', *, *, #96654, .F. ) ;
#86658=CARTESIAN_POINT ( 'NONE',  ( -3.482456173223098528, 20.84670800329844198, 11.49999999999998934 ) ) ;
#86660=CARTESIAN_POINT ( 'NONE',  ( -51.54603119510975517, -25.26041023287835330, 7.131525817319249505 ) ) ;
#86661=CARTESIAN_POINT ( 'NONE',  ( -121.5924648986724321, -23.48783264082477018, -1.443836473390087694 ) ) ;
#86663=CARTESIAN_POINT ( 'NONE',  ( -47.62287095715005592, -24.33927499327854704, 9.819080762295826048 ) ) ;
#86664=CARTESIAN_POINT ( 'NONE',  ( -17.05807961832342912, 14.25954964135033265, -1.500000000000002220 ) ) ;
#86665=CARTESIAN_POINT ( 'NONE',  ( -49.57708068730813267, -25.13941455849516515, 7.373516634279884130 ) ) ;
#86666=ADVANCED_FACE ( 'NONE', ( #63264 ), #38403, .T. ) ;
#86668=ORIENTED_EDGE ( 'NONE', *, *, #100198, .T. ) ;
#86669=CARTESIAN_POINT ( 'NONE',  ( -110.6228709571500843, -23.47596703998600631, 11.44779298504227860 ) ) ;
#86670=CARTESIAN_POINT ( 'NONE',  ( -37.61806166826795561, -23.48783264082478084, -1.443836473390075703 ) ) ;
#86671=CARTESIAN_POINT ( 'NONE',  ( -40.09687989520371332, -25.30461012899484174, 5.519286114388885167 ) ) ;
#86672=CARTESIAN_POINT ( 'NONE',  ( -100.5881607692819699, -24.63355581998384380, 0.9682620441943933232 ) ) ;
#86673=CARTESIAN_POINT ( 'NONE',  ( -33.52287095715006160, -24.65952944569303895, 1.056160979905690134 ) ) ;
#86674=CARTESIAN_POINT ( 'NONE',  ( 15.68791110202092476, 11.56419973807686219, -1.500000000000002220 ) ) ;
#86676=CARTESIAN_POINT ( 'NONE',  ( 10.55508701655855575, -18.62573008410804221, -1.500000000000002220 ) ) ;
#86678=CARTESIAN_POINT ( 'NONE',  ( -59.56094173781918499, -25.21083105912962097, 3.409327675794633805 ) ) ;
#86680=CARTESIAN_POINT ( 'NONE',  ( -51.49050306338898508, -24.51314013834315730, 0.6176544820404109570 ) ) ;
#86681=CARTESIAN_POINT ( 'NONE',  ( -101.2457357660222641, -25.27360070449644880, 3.734960848544197187 ) ) ;
#86682=CARTESIAN_POINT ( 'NONE',  ( -21.73129956901698989, 6.668506094012985663, -1.500000000000002220 ) ) ;
#86683=DIRECTION ( 'NONE',  ( -3.773278334453079030E-23, 0.9999999999976377785, 2.173523156925979128E-06 ) ) ;
#86684=CARTESIAN_POINT ( 'NONE',  ( -73.22287095715006444, -23.47593901973090169, -1.443836447538997536 ) ) ;
#86685=CARTESIAN_POINT ( 'NONE',  ( -7.150643268323968904, -18.52920452239153448, 11.49999999999999645 ) ) ;
#86686=CARTESIAN_POINT ( 'NONE',  ( -123.5570543124543548, -23.48786465467241413, 11.44779295918253759 ) ) ;
#86688=FACE_OUTER_BOUND ( 'NONE', #50977, .T. ) ;
#86689=ORIENTED_EDGE ( 'NONE', *, *, #95764, .T. ) ;
#86691=CARTESIAN_POINT ( 'NONE',  ( -123.5228709571501042, -23.48783264082477018, -1.443836473390084141 ) ) ;
#86693=CARTESIAN_POINT ( 'NONE',  ( -63.55620429048339304, -23.48786465467241058, 11.44779295918254824 ) ) ;
#86694=CARTESIAN_POINT ( 'NONE',  ( -1.126084586642228436, -21.63456646517454729, -1.500000000000002220 ) ) ;
#86695=CARTESIAN_POINT ( 'NONE',  ( -17.22176335520693158, -9.073154711715998744, -1.500000000000002220 ) ) ;
#86696=CARTESIAN_POINT ( 'NONE',  ( -112.6228709571500559, -29.50250243563736774, 8.947779886222136270 ) ) ;
#86697=ORIENTED_EDGE ( 'NONE', *, *, #30636, .F. ) ;
#86698=VECTOR ( 'NONE', #95688, 1000.000000000000114 ) ;
#86699=CARTESIAN_POINT ( 'NONE',  ( 8.094744887094867281, -18.73235182305680624, 11.49999999999999645 ) ) ;
#86701=CARTESIAN_POINT ( 'NONE',  ( -104.5562042904834072, -23.48783264082478084, -1.443836473390061936 ) ) ;
#86704=DIRECTION ( 'NONE',  ( 0.000000000000000000, 0.9999999999976377785, 2.173523156925979975E-06 ) ) ;
#86707=B_SPLINE_CURVE_WITH_KNOTS ( 'NONE', 3,
 ( #83233, #83731, #84229, #14716, #29947, #53800 ),
 .UNSPECIFIED., .F., .F.,
 ( 4, 2, 4 ),
 ( 0.000000000000000000, 0.001380764517853246432, 0.002761529035706492864 ),
 .UNSPECIFIED. ) ;
#86708=LINE ( 'NONE', #17198, #68954 ) ;
#86709=CARTESIAN_POINT ( 'NONE',  ( 10.48293302797296356, 17.13603372422173976, 11.49999999999998934 ) ) ;
#86710=ADVANCED_FACE ( 'NONE', ( #17063 ), #77451, .F. ) ;
#86712=ORIENTED_EDGE ( 'NONE', *, *, #30538, .T. ) ;
#86713=FACE_OUTER_BOUND ( 'NONE', #3604, .T. ) ;
#86715=CARTESIAN_POINT ( 'NONE',  ( -22.94451526424785115, -1.264959178018935315, 11.49999999999999645 ) ) ;
#86716=CARTESIAN_POINT ( 'NONE',  ( 21.15473741701296362, -8.388382055385795510, -1.500000000000002220 ) ) ;
#86717=ORIENTED_EDGE ( 'NONE', *, *, #97324, .T. ) ;
#86718=CARTESIAN_POINT ( 'NONE',  ( -45.52287095715004739, -23.48783264082477018, -1.443836473390097019 ) ) ;
#86720=CARTESIAN_POINT ( 'NONE',  ( -90.54595667564740324, -24.63355581998384736, 0.9682620441943978751 ) ) ;
#86723=EDGE_CURVE ( 'NONE', #48372, #13321, #78733, .T. ) ;
#86725=EDGE_CURVE ( 'NONE', #27806, #61427, #59548, .T. ) ;
#86726=CARTESIAN_POINT ( 'NONE',  ( -121.5228709571500616, -24.64898659630529565, 1.056161002820833028 ) ) ;
#86727=CARTESIAN_POINT ( 'NONE',  ( -39.62287095715005592, -24.65952944569304606, 1.056160979905692354 ) ) ;
#86728=CARTESIAN_POINT ( 'NONE',  ( -98.89580656140421411, -25.25460702255793777, 6.002154820449574935 ) ) ;
#86729=VERTEX_POINT ( 'NONE', #47530 ) ;
#86730=CARTESIAN_POINT ( 'NONE',  ( -14.54385459823299875, 14.27422344363935025, 11.49999999999998934 ) ) ;
#86731=ORIENTED_EDGE ( 'NONE', *, *, #60438, .F. ) ;
#86732=ORIENTED_EDGE ( 'NONE', *, *, #72940, .F. ) ;
#86733=CARTESIAN_POINT ( 'NONE',  ( -19.99251892732797486, -11.32171818645973538, 11.49999999999998934 ) ) ;
#86737=CARTESIAN_POINT ( 'NONE',  ( -108.6335398323394230, -23.48786465467241413, 11.44779295918253759 ) ) ;
#86740=CARTESIAN_POINT ( 'NONE',  ( -78.55620429048339304, -24.64965694238574656, 8.947790433994198267 ) ) ;
#86741=CARTESIAN_POINT ( 'NONE',  ( -119.1722160062776226, -25.27149295872829882, 5.922904214524349342 ) ) ;
#86742=CARTESIAN_POINT ( 'NONE',  ( -9.236746577462426444, 19.23066362772381055, 11.49999999999999645 ) ) ;
#86743=VERTEX_POINT ( 'NONE', #89085 ) ;
#86745=CARTESIAN_POINT ( 'NONE',  ( 10.78255534502030777, 19.45608938089507234, -1.500000000000002220 ) ) ;
#86746=CARTESIAN_POINT ( 'NONE',  ( 20.62939718826500979, -0.8834638802319035866, 11.49999999999998934 ) ) ;
#86748=ORIENTED_EDGE ( 'NONE', *, *, #94322, .F. ) ;
#86749=FACE_OUTER_BOUND ( 'NONE', #92119, .T. ) ;
#86750=CARTESIAN_POINT ( 'NONE',  ( -95.58789313718423841, -24.63419186844610920, 9.035850630976922204 ) ) ;
#86752=CARTESIAN_POINT ( 'NONE',  ( -73.62287095715005592, -29.50250243563736774, 8.947779886222143375 ) ) ;
#86756=CARTESIAN_POINT ( 'NONE',  ( -16.98601802344612111, -12.12340321765213069, -1.500000000000002220 ) ) ;
#86757=CARTESIAN_POINT ( 'NONE',  ( -6.661741538832703036, 20.79550341630197607, 11.49999999999999645 ) ) ;
#86760=CARTESIAN_POINT ( 'NONE',  ( -15.60622653811170402, 16.18669697583415967, 11.49999999999998934 ) ) ;
#86761=EDGE_CURVE ( 'NONE', #50194, #98189, #80032, .T. ) ;
#86762=EDGE_CURVE ( 'NONE', #55399, #3242, #72858, .T. ) ;
#86763=CARTESIAN_POINT ( 'NONE',  ( -118.5911711092949332, -23.96169478059713853, 10.65365249895717170 ) ) ;
#86764=CARTESIAN_POINT ( 'NONE',  ( -125.5228709571500616, -29.50248789122583659, 2.256150453626215580 ) ) ;
#86765=CARTESIAN_POINT ( 'NONE',  ( -59.52287095715006160, -23.47596703998600631, 11.44779298504228926 ) ) ;
#86767=VECTOR ( 'NONE', #20301, 1000.000000000000114 ) ;
#86768=ORIENTED_EDGE ( 'NONE', *, *, #51977, .F. ) ;
#86770=CARTESIAN_POINT ( 'NONE',  ( -100.0836892525862254, -25.26221310139842302, 7.064315631329017187 ) ) ;
#86772=CARTESIAN_POINT ( 'NONE',  ( -13.24026558610970916, 16.85365899302435722, -1.500000000000002220 ) ) ;
#86773=CARTESIAN_POINT ( 'NONE',  ( -21.65924713590726469, 5.634197536097032888, 11.49999999999999645 ) ) ;
#86774=VERTEX_POINT ( 'NONE', #1852 ) ;
#86776=CARTESIAN_POINT ( 'NONE',  ( 13.75562813033083742, -15.94169299924578453, 11.49999999999998934 ) ) ;
#86777=CARTESIAN_POINT ( 'NONE',  ( -30.55373813234560032, -24.38552179065370851, 9.702671485061733492 ) ) ;
#86778=CARTESIAN_POINT ( 'NONE',  ( 18.80405327530603543, -6.659971710459020144, -1.500000000000002220 ) ) ;
#86779=FACE_OUTER_BOUND ( 'NONE', #45934, .T. ) ;
#86781=CARTESIAN_POINT ( 'NONE',  ( -20.36895902721504825, -8.506870616244709637, -1.500000000000002220 ) ) ;
#86783=CARTESIAN_POINT ( 'NONE',  ( -65.53712136039511904, -24.73531770709095312, 8.716586749053508498 ) ) ;
#86784=ADVANCED_FACE ( 'NONE', ( #27189 ), #34302, .F. ) ;
#86786=CARTESIAN_POINT ( 'NONE',  ( 12.46380520747237419, 16.70348211664046900, 11.49999999999999645 ) ) ;
#86788=DIRECTION ( 'NONE',  ( 0.000000000000000000, -2.173523156925980399E-06, 0.9999999999976378895 ) ) ;
#86790=CARTESIAN_POINT ( 'NONE',  ( -12.43717309395686499, -17.31322327496724611, -1.500000000000002220 ) ) ;
#86791=CARTESIAN_POINT ( 'NONE',  ( -81.52287095715006160, -23.94994826722564696, -0.6494450866342743600 ) ) ;
#86792=CARTESIAN_POINT ( 'NONE',  ( -33.62287095715005592, -29.50248528299804818, 1.056150453629029817 ) ) ;
#86793=EDGE_CURVE ( 'NONE', #62739, #59306, #15842, .T. ) ;
#86794=CARTESIAN_POINT ( 'NONE',  ( -96.52287095715006160, -23.48786465467241769, 11.44779295918254114 ) ) ;
#86796=CARTESIAN_POINT ( 'NONE',  ( -20.50338545487000275, 9.463669735852004550, -1.500000000000002220 ) ) ;
#86797=AXIS2_PLACEMENT_3D ( 'NONE', #36692, #98578, #60047 ) ;
#86798=ADVANCED_FACE ( 'NONE', ( #11951 ), #49038, .F. ) ;
#86799=CARTESIAN_POINT ( 'NONE',  ( -51.52287095715008292, -23.96177878511308634, 10.65340807706329862 ) ) ;
#86800=ORIENTED_EDGE ( 'NONE', *, *, #5024, .F. ) ;
#86802=CARTESIAN_POINT ( 'NONE',  ( -122.6228709571500417, -24.64898659630368627, 1.056161002820833028 ) ) ;
#86803=CARTESIAN_POINT ( 'NONE',  ( -8.025172913017740939, -17.94849717234452768, 11.49999999999999645 ) ) ;
#86806=CARTESIAN_POINT ( 'NONE',  ( -119.5228709571500758, -24.64965694238408034, 8.947790433994191162 ) ) ;
#86807=ORIENTED_EDGE ( 'NONE', *, *, #46281, .T. ) ;
#86811=DIRECTION ( 'NONE',  ( 0.000000000000000000, -2.173523156925979552E-06, 0.9999999999976378895 ) ) ;
#86816=CARTESIAN_POINT ( 'NONE',  ( 19.69962056004252560, 1.334664424591413434, 11.49999999999998934 ) ) ;
#86818=CARTESIAN_POINT ( 'NONE',  ( -1.055277534996966970, 20.15608268182561247, 11.49999999999999645 ) ) ;
#86824=CARTESIAN_POINT ( 'NONE',  ( -69.75867036063475268, -25.12509700652633171, 2.913778224305814124 ) ) ;
#86825=DIRECTION ( 'NONE',  ( -3.773278334453079030E-23, 0.9999999999976377785, 2.173523156925979128E-06 ) ) ;
#86826=CARTESIAN_POINT ( 'NONE',  ( -58.52287095715006160, -24.64898659630528499, 1.056161002820822592 ) ) ;
#86827=CARTESIAN_POINT ( 'NONE',  ( 16.76344175524385705, -10.90933549886441156, 11.49999999999998934 ) ) ;
#86828=CARTESIAN_POINT ( 'NONE',  ( -99.49608100277511369, -25.27532937069960184, 3.179641110928470127 ) ) ;
#86829=CARTESIAN_POINT ( 'NONE',  ( -116.6272977626530292, -23.96169478059714208, 10.65365249895717348 ) ) ;
#86831=EDGE_CURVE ( 'NONE', #80901, #48067, #31674, .T. ) ;
#86832=LINE ( 'NONE', #16823, #24281 ) ;
#86833=CARTESIAN_POINT ( 'NONE',  ( -35.63364392773276990, -24.73486907724918282, 1.287355809206967461 ) ) ;
#86834=CARTESIAN_POINT ( 'NONE',  ( -48.58953762381672448, -24.64965694238407323, 8.947790433994656567 ) ) ;
#86835=CARTESIAN_POINT ( 'NONE',  ( -118.7287160163637481, -25.33540118152307841, 3.690489000554330712 ) ) ;
#86837=CARTESIAN_POINT ( 'NONE',  ( -45.52287095715006160, -23.47596703998600631, 11.44779298504229104 ) ) ;
#86838=PLANE ( 'NONE',  #9650 ) ;
#86840=CARTESIAN_POINT ( 'NONE',  ( -2.359408512905806443, -20.17289352931189583, -1.500000000000002220 ) ) ;
#86842=CARTESIAN_POINT ( 'NONE',  ( -34.53217422167019635, -24.51314013834315375, 0.6176544820404091807 ) ) ;
#86843=CARTESIAN_POINT ( 'NONE',  ( -59.55981053866136676, -23.73791477778911840, 11.05961554403171299 ) ) ;
#86844=AXIS2_PLACEMENT_3D ( 'NONE', #41036, #18676, #79076 ) ;
#86846=DIRECTION ( 'NONE',  ( 0.000000000000000000, -0.9999999999976377785, -2.173523156925979128E-06 ) ) ;
#86847=CARTESIAN_POINT ( 'NONE',  ( 12.02422309597069017, 16.21794576832014556, -1.500000000000002220 ) ) ;
#86848=CARTESIAN_POINT ( 'NONE',  ( -20.79277273739468512, 3.736189789763188607, 11.49999999999999645 ) ) ;
#86849=CARTESIAN_POINT ( 'NONE',  ( 19.88262469969689050, -9.776007750257504014, -1.500000000000002220 ) ) ;
#86850=CARTESIAN_POINT ( 'NONE',  ( -14.32454646668868747, 14.77526322620295929, 11.49999999999998934 ) ) ;
#86851=AXIS2_PLACEMENT_3D ( 'NONE', #76841, #68266, #62156 ) ;
#86852=EDGE_CURVE ( 'NONE', #46688, #16912, #11024, .T. ) ;
#86853=FACE_OUTER_BOUND ( 'NONE', #61478, .T. ) ;
#86855=CARTESIAN_POINT ( 'NONE',  ( -43.52287095715006160, -24.64898659630528854, 1.056161002820819261 ) ) ;
#86857=CARTESIAN_POINT ( 'NONE',  ( -36.62287095715004170, -23.47596703998600276, 11.44779298504227505 ) ) ;
#86858=CARTESIAN_POINT ( 'NONE',  ( -109.5228709571500332, -23.95044443724992789, 10.65354141964649237 ) ) ;
#86859=EDGE_LOOP ( 'NONE', ( #91601, #34324, #48943, #84928 ) ) ;
#86860=AXIS2_PLACEMENT_3D ( 'NONE', #32502, #53845, #1562 ) ;
#86863=ORIENTED_EDGE ( 'NONE', *, *, #31347, .T. ) ;
#86865=CARTESIAN_POINT ( 'NONE',  ( -28.92287090416851214, -23.34271810397723357, -1.443836447538997314 ) ) ;
#86866=CARTESIAN_POINT ( 'NONE',  ( -108.5228709571500616, -24.64965694238408034, 8.947790433994192938 ) ) ;
#86867=CARTESIAN_POINT ( 'NONE',  ( -10.41657757243416604, 17.86655067824183618, -1.500000000000002220 ) ) ;
#86869=CARTESIAN_POINT ( 'NONE',  ( -6.031157642910047301, -20.80930661755759203, 11.49999999999999645 ) ) ;
#86870=ORIENTED_EDGE ( 'NONE', *, *, #84970, .T. ) ;
#86872=CARTESIAN_POINT ( 'NONE',  ( -99.07956767207025450, -25.29825536674003672, 5.429397271924422341 ) ) ;
#86873=CARTESIAN_POINT ( 'NONE',  ( -33.52287095715006160, -29.50247984919015209, -1.443849546365062242 ) ) ;
#86874=CARTESIAN_POINT ( 'NONE',  ( 18.65981798208652265, 12.38953945867474360, 11.49999999999998934 ) ) ;
#86876=AXIS2_PLACEMENT_3D ( 'NONE', #79979, #47545, #63789 ) ;
#86878=CARTESIAN_POINT ( 'NONE',  ( -46.52287095715006160, -29.50250243563736774, 8.947779886222146928 ) ) ;
#86879=DIRECTION ( 'NONE',  ( -1.000000000000000000, -3.773278334444166432E-23, -8.201307841325785021E-29 ) ) ;
#86880=ORIENTED_EDGE ( 'NONE', *, *, #15219, .T. ) ;
#86882=CARTESIAN_POINT ( 'NONE',  ( -35.61370034920652472, -23.85049219812685095, 10.88485053497527488 ) ) ;
#86884=ORIENTED_EDGE ( 'NONE', *, *, #73080, .T. ) ;
#86886=CARTESIAN_POINT ( 'NONE',  ( -45.52287095715006870, -24.51254535375846189, 9.355368624242117903 ) ) ;
#86888=PLANE ( 'NONE',  #17951 ) ;
#86889=CARTESIAN_POINT ( 'NONE',  ( -21.21068194950259311, 0.7780057951688260642, -1.500000000000002220 ) ) ;
#86890=ORIENTED_EDGE ( 'NONE', *, *, #48589, .F. ) ;
#86891=CARTESIAN_POINT ( 'NONE',  ( -50.48315116308123862, -24.73486907724918282, 1.287355809206963464 ) ) ;
#86892=CARTESIAN_POINT ( 'NONE',  ( 1.801620404824296084, -21.73869551012647605, 11.49999999999998934 ) ) ;
#86893=CARTESIAN_POINT ( 'NONE',  ( -103.5131093972200773, -24.35071581493543391, 9.817618358456027039 ) ) ;
#86895=LINE ( 'NONE', #17387, #21013 ) ;
#86897=CARTESIAN_POINT ( 'NONE',  ( 21.05697796394607835, 5.830696701215154043, -1.500000000000002220 ) ) ;
#86900=CARTESIAN_POINT ( 'NONE',  ( -65.62287095715007013, -24.63287334234177806, 0.9662140553045478475 ) ) ;
#86901=CARTESIAN_POINT ( 'NONE',  ( -85.50201578033416183, -24.63419186844611275, 9.035850630976915099 ) ) ;
#86902=EDGE_CURVE ( 'NONE', #40713, #95088, #8686, .T. ) ;
#86903=VERTEX_POINT ( 'NONE', #91069 ) ;
#86905=ORIENTED_EDGE ( 'NONE', *, *, #98545, .T. ) ;
#86906=EDGE_CURVE ( 'NONE', #58835, #30291, #52518, .T. ) ;
#86907=VERTEX_POINT ( 'NONE', #83451 ) ;
#86908=CARTESIAN_POINT ( 'NONE',  ( -89.46310519935767047, -25.12049752546737480, 2.832404795212219106 ) ) ;
#86909=CARTESIAN_POINT ( 'NONE',  ( -82.63299566570569255, -24.15543982623907482, -0.2315651400026497997 ) ) ;
#86910=CARTESIAN_POINT ( 'NONE',  ( 20.49604761983493972, 5.601127818285958071, -1.500000000000002220 ) ) ;
#86911=CARTESIAN_POINT ( 'NONE',  ( -27.68651082257923335, -29.50249951851372643, 7.605662314874230390 ) ) ;
#86913=EDGE_CURVE ( 'NONE', #98477, #27379, #95845, .T. ) ;
#86915=CARTESIAN_POINT ( 'NONE',  ( -91.52287095715003318, -23.48783264082477018, -1.443836473390089248 ) ) ;
#86916=CARTESIAN_POINT ( 'NONE',  ( 17.07123823605233781, 9.195568589125342029, -1.500000000000002220 ) ) ;
#86917=CARTESIAN_POINT ( 'NONE',  ( -45.49175542960804819, -24.40034930558990922, 0.3402023900116019073 ) ) ;
#86918=ORIENTED_EDGE ( 'NONE', *, *, #22848, .T. ) ;
#86919=CARTESIAN_POINT ( 'NONE',  ( 2.628080361126900133, -19.32819128710564272, 11.49999999999999645 ) ) ;
#86921=CARTESIAN_POINT ( 'NONE',  ( -68.52287095715007581, -23.47593901973090524, -1.443836447538997092 ) ) ;
#86923=EDGE_CURVE ( 'NONE', #54685, #89496, #66770, .T. ) ;
#86925=CARTESIAN_POINT ( 'NONE',  ( -89.58353647075207959, -24.65952944569304250, 1.056160979905701902 ) ) ;
#86928=CARTESIAN_POINT ( 'NONE',  ( -81.79035934495350091, -25.03155870187092447, 6.685840044562571194 ) ) ;
#86929=CARTESIAN_POINT ( 'NONE',  ( -19.44079195400435012, 3.002763184081948200, -1.500000000000002220 ) ) ;
#86930=B_SPLINE_CURVE_WITH_KNOTS ( 'NONE', 3,
 ( #20686, #91693, #74969, #67384, #4973, #44540 ),
 .UNSPECIFIED., .F., .F.,
 ( 4, 2, 4 ),
 ( 0.000000000000000000, 0.001380764517853249251, 0.002761529035706498502 ),
 .UNSPECIFIED. ) ;
#86931=VERTEX_POINT ( 'NONE', #98176 ) ;
#86932=CARTESIAN_POINT ( 'NONE',  ( -109.6228709571500559, -29.50247984919015209, -1.443849546365048253 ) ) ;
#86933=CARTESIAN_POINT ( 'NONE',  ( -23.06710473063640165, 0.7821689226722955413, -1.500000000000002220 ) ) ;
#86937=CARTESIAN_POINT ( 'NONE',  ( -51.52287095715006870, -29.50248528299804818, 1.056150453629033370 ) ) ;
#86938=CARTESIAN_POINT ( 'NONE',  ( -109.7112239897570163, -25.13124142841114050, 2.950745540745953743 ) ) ;
#86939=CARTESIAN_POINT ( 'NONE',  ( -97.58870659920341950, -24.35071581493544102, 9.817618358456025263 ) ) ;
#86940=CARTESIAN_POINT ( 'NONE',  ( -79.91702284995605510, -25.31249729222309242, 5.276660411446114196 ) ) ;
#86945=CARTESIAN_POINT ( 'NONE',  ( -111.3663525145439053, -25.29779355382247985, 4.214194357447069272 ) ) ;
#86946=CARTESIAN_POINT ( 'NONE',  ( -19.91179686852411734, 0.6080443046932394457, 11.49999999999998934 ) ) ;
#86947=B_SPLINE_CURVE_WITH_KNOTS ( 'NONE', 3,
 ( #32653, #16929, #94052, #70721, #46383, #77317 ),
 .UNSPECIFIED., .F., .F.,
 ( 4, 2, 4 ),
 ( 0.000000000000000000, 0.001380901958385393966, 0.002761803916770787931 ),
 .UNSPECIFIED. ) ;
#86948=DIRECTION ( 'NONE',  ( -1.000000000000000000, -3.773278334444166432E-23, -8.201307841325785021E-29 ) ) ;
#86949=CARTESIAN_POINT ( 'NONE',  ( -11.05534852661189937, -16.44151763790470966, -1.500000000000002220 ) ) ;
#86954=CARTESIAN_POINT ( 'NONE',  ( -35.62287095715005592, -24.91570333823099404, 8.075032458375558164 ) ) ;
#86955=CARTESIAN_POINT ( 'NONE',  ( -7.464567774302189207, 19.34240081622845153, 11.49999999999999645 ) ) ;
#86956=DIRECTION ( 'NONE',  ( -3.773278334444167608E-23, 1.000000000000000000, 0.000000000000000000 ) ) ;
#86957=CARTESIAN_POINT ( 'NONE',  ( -78.52287095715006160, -23.47596703998600631, 11.44779298504228571 ) ) ;
#86958=CARTESIAN_POINT ( 'NONE',  ( 22.53581206741051446, 3.480912172000575122, 11.49999999999999645 ) ) ;
#86959=ORIENTED_EDGE ( 'NONE', *, *, #73518, .T. ) ;
#86960=CARTESIAN_POINT ( 'NONE',  ( -69.54473523537089363, -24.34968618360934300, 0.1864209137778826408 ) ) ;
#86963=CARTESIAN_POINT ( 'NONE',  ( 17.48260522047220888, -10.12088315688240314, 11.49999999999998934 ) ) ;
#86965=CARTESIAN_POINT ( 'NONE',  ( -110.5228709571500616, -24.83620972994592435, 8.398175272781363887 ) ) ;
#86966=AXIS2_PLACEMENT_3D ( 'NONE', #86878, #140, #33098 ) ;
#86968=CARTESIAN_POINT ( 'NONE',  ( -127.5228709571499763, -23.48783264082477373, -1.443836473390082586 ) ) ;
#86969=CARTESIAN_POINT ( 'NONE',  ( -30.57287095715006231, -23.47596702059239604, 11.43887032355635647 ) ) ;
#86970=CARTESIAN_POINT ( 'NONE',  ( 1.534201407001029027, 19.92515851932037663, -1.500000000000002220 ) ) ;
#86972=CARTESIAN_POINT ( 'NONE',  ( -20.92093621315066443, -1.481899440790641842, 11.49999999999999645 ) ) ;
#86976=CARTESIAN_POINT ( 'NONE',  ( 1.153593019990587942, -22.03401787307112869, -1.500000000000002220 ) ) ;
#86977=CARTESIAN_POINT ( 'NONE',  ( -127.4728709571500360, -25.40674640480649416, 5.000950437805943061 ) ) ;
#86978=ORIENTED_EDGE ( 'NONE', *, *, #14947, .F. ) ;
#86979=DIRECTION ( 'NONE',  ( 0.000000000000000000, -0.9999999999976377785, -2.173523156925979975E-06 ) ) ;
#86980=CARTESIAN_POINT ( 'NONE',  ( -35.62287095715005592, -23.47593901973091235, -1.443836447539011525 ) ) ;
#86983=DIRECTION ( 'NONE',  ( 0.000000000000000000, -2.173523156925980399E-06, 0.9999999999976378895 ) ) ;
#86985=ORIENTED_EDGE ( 'NONE', *, *, #96884, .F. ) ;
#86986=ADVANCED_FACE ( 'NONE', ( #38275 ), #38860, .T. ) ;
#86987=ORIENTED_EDGE ( 'NONE', *, *, #69830, .T. ) ;
#86988=CARTESIAN_POINT ( 'NONE',  ( -118.5228709571501184, -24.66019654487200441, 8.947790411086110396 ) ) ;
#86990=CARTESIAN_POINT ( 'NONE',  ( -94.62287095715005592, -23.47596703998600631, 11.44779298504227860 ) ) ;
#86991=CARTESIAN_POINT ( 'NONE',  ( -20.41219973434085944, 2.133827299322149429, -1.500000000000002220 ) ) ;
#86992=EDGE_CURVE ( 'NONE', #73682, #59253, #99427, .T. ) ;
#86993=ORIENTED_EDGE ( 'NONE', *, *, #50274, .T. ) ;
#86994=CARTESIAN_POINT ( 'NONE',  ( -116.5228709571500332, -24.66019654487200086, 8.947790411086113949 ) ) ;
#86996=CARTESIAN_POINT ( 'NONE',  ( -41.52287095715008292, -23.95044443724991723, 10.65354141964649237 ) ) ;
#86997=CARTESIAN_POINT ( 'NONE',  ( -20.55042600948665310, 8.738301046694649798, -1.500000000000002220 ) ) ;
#87001=CARTESIAN_POINT ( 'NONE',  ( -0.07181233839971860877, -22.12033284636825314, 9.440663514584120009 ) ) ;
#87002=CARTESIAN_POINT ( 'NONE',  ( -55.52287095715006870, -29.50248528299804818, 1.056150453629034924 ) ) ;
#87003=VERTEX_POINT ( 'NONE', #78329 ) ;
#87006=CARTESIAN_POINT ( 'NONE',  ( 2.550444227103870531, -20.70361394434535285, -1.500000000000002220 ) ) ;
#87008=LINE ( 'NONE', #80401, #47394 ) ;
#87012=CARTESIAN_POINT ( 'NONE',  ( -32.66693324679340549, -24.96126789006231306, 2.105721083233587532 ) ) ;
#87013=CARTESIAN_POINT ( 'NONE',  ( 18.99863377428308198, 9.053671573812124507, -1.500000000000002220 ) ) ;
#87014=EDGE_LOOP ( 'NONE', ( #61496, #98329, #19495, #67778 ) ) ;
#87015=AXIS2_PLACEMENT_3D ( 'NONE', #9897, #55592, #71310 ) ;
#87016=DIRECTION ( 'NONE',  ( 0.000000000000000000, -2.173523156925979552E-06, 0.9999999999976378895 ) ) ;
#87018=CARTESIAN_POINT ( 'NONE',  ( -105.5228709571500758, -25.00182538069145366, 7.747789668545101094 ) ) ;
#87019=VECTOR ( 'NONE', #96624, 1000.000000000000114 ) ;
#87020=CARTESIAN_POINT ( 'NONE',  ( -86.50205518092207058, -24.66019654487200086, 8.947790411086117501 ) ) ;
#87021=CARTESIAN_POINT ( 'NONE',  ( -73.55620429048342146, -24.65952944569304606, 1.056160979905697461 ) ) ;
#87022=LINE ( 'NONE', #25113, #52908 ) ;
#87023=CARTESIAN_POINT ( 'NONE',  ( -65.62287095715005592, -25.00182538069145721, 7.747789668545100206 ) ) ;
#87024=CARTESIAN_POINT ( 'NONE',  ( -13.56020932195406203, -17.60290058955388659, 11.49999999999999645 ) ) ;
#87026=DIRECTION ( 'NONE',  ( -3.773278334453079618E-23, 0.9999999999976377785, 2.173523156925979975E-06 ) ) ;
#87027=CARTESIAN_POINT ( 'NONE',  ( -37.62287095715005592, -23.48786465467240347, 11.44779295918255180 ) ) ;
#87028=VERTEX_POINT ( 'NONE', #55017 ) ;
#87029=CARTESIAN_POINT ( 'NONE',  ( -22.58250372949163420, -2.080990182559540269, -1.500000000000002220 ) ) ;
#87030=DIRECTION ( 'NONE',  ( -3.773278334453079618E-23, 0.9999999999976377785, 2.173523156925978705E-06 ) ) ;
#87031=VERTEX_POINT ( 'NONE', #85955 ) ;
#87033=ORIENTED_EDGE ( 'NONE', *, *, #15686, .T. ) ;
#87035=B_SPLINE_CURVE_WITH_KNOTS ( 'NONE', 3,
 ( #15818, #61517, #85840, #54398, #94452, #31548, #76701, #46277 ),
 .UNSPECIFIED., .F., .F.,
 ( 4, 2, 2, 4 ),
 ( 6.391158118973814098E-06, 0.002007136338672923983, 0.003007508928949901694, 0.004007881519226879838 ),
 .UNSPECIFIED. ) ;
#87036=CARTESIAN_POINT ( 'NONE',  ( -10.68008619461380704, -17.10268970254769982, 11.49999999999998934 ) ) ;
#87037=CARTESIAN_POINT ( 'NONE',  ( -84.52287095715006160, -23.47596703998600631, 11.44779298504228571 ) ) ;
#87038=EDGE_LOOP ( 'NONE', ( #12038, #2216, #89437, #36641 ) ) ;
#87039=CARTESIAN_POINT ( 'NONE',  ( -130.5728709571500303, -25.40560073940965324, 5.290910518220999670 ) ) ;
#87040=CARTESIAN_POINT ( 'NONE',  ( 20.53814608839396527, -8.957171556794316203, -1.500000000000002220 ) ) ;
#87042=ORIENTED_EDGE ( 'NONE', *, *, #30893, .F. ) ;
#87043=CARTESIAN_POINT ( 'NONE',  ( -112.5553928173894036, -23.96169478059713498, 10.65365249895717170 ) ) ;
#87044=CARTESIAN_POINT ( 'NONE',  ( -48.55620429048340014, -24.66019654487199020, 8.947790411086135265 ) ) ;
#87045=CARTESIAN_POINT ( 'NONE',  ( -61.52287095715007581, -23.72773821059535848, 11.05748984161097326 ) ) ;
#87049=EDGE_CURVE ( 'NONE', #63165, #39828, #44998, .T. ) ;
#87050=CARTESIAN_POINT ( 'NONE',  ( -19.49195742049215241, -1.735909528584683947, 11.49999999999998934 ) ) ;
#87051=CARTESIAN_POINT ( 'NONE',  ( -46.51386545360935543, -23.73766607897669800, -1.055555164236460230 ) ) ;
#87053=CARTESIAN_POINT ( 'NONE',  ( 19.32660459246815421, -9.429101867163046435, -1.500000000000002220 ) ) ;
#87055=CARTESIAN_POINT ( 'NONE',  ( -36.62287095715005592, -23.47593901973091235, -1.443836447539011525 ) ) ;
#87057=CARTESIAN_POINT ( 'NONE',  ( -123.5228709571500616, -23.48786465467242479, 11.44779295918253759 ) ) ;
#87058=ADVANCED_FACE ( 'NONE', ( #6827 ), #61140, .T. ) ;
#87059=DIRECTION ( 'NONE',  ( -3.773278334453080206E-23, 0.9999999999976377785, 2.173523156925979975E-06 ) ) ;
#87060=CARTESIAN_POINT ( 'NONE',  ( 22.81499323874321661, -2.031749852351878882, -1.500000000000002220 ) ) ;
#87062=CARTESIAN_POINT ( 'NONE',  ( -92.58953762381672448, -23.47593901973091235, -1.443836447539002865 ) ) ;
#87063=CARTESIAN_POINT ( 'NONE',  ( -120.5228709571500616, -29.50248789122583659, 2.256150453626215580 ) ) ;
#87064=CARTESIAN_POINT ( 'NONE',  ( -15.22981678846565856, -13.14137338692033907, 11.49999999999999645 ) ) ;
#87065=CARTESIAN_POINT ( 'NONE',  ( -40.52287095715007581, -25.00182538069145011, 7.747789668545104647 ) ) ;
#87071=CARTESIAN_POINT ( 'NONE',  ( 17.96171645398845129, 8.431260308876343146, -1.500000000000002220 ) ) ;
#87072=CARTESIAN_POINT ( 'NONE',  ( 21.40858030128615397, -3.853468400179685727, -1.500000000000002220 ) ) ;
#87074=CARTESIAN_POINT ( 'NONE',  ( 10.60981200654714307, 16.52409317135366607, -1.500000000000002220 ) ) ;
#87076=CARTESIAN_POINT ( 'NONE',  ( -60.52287095715008292, -23.48783264082477018, -1.443836473390092801 ) ) ;
#87077=CARTESIAN_POINT ( 'NONE',  ( -54.52287095715007581, -23.73934037231755667, 11.05740245334329330 ) ) ;
#87078=CARTESIAN_POINT ( 'NONE',  ( -103.5228709571501042, -23.47593901973090524, -1.443836447538996204 ) ) ;
#87079=LINE ( 'NONE', #48541, #34544 ) ;
#87080=CARTESIAN_POINT ( 'NONE',  ( -20.17529555308526668, -4.016306826964139098, 11.49999999999999645 ) ) ;
#87081=DIRECTION ( 'NONE',  ( -3.773278334444166432E-23, 1.000000000000000000, 0.000000000000000000 ) ) ;
#87083=CARTESIAN_POINT ( 'NONE',  ( -47.62287095715004881, -24.51283580621364777, 0.6167428607019750375 ) ) ;
#87084=CARTESIAN_POINT ( 'NONE',  ( 14.59886444729927923, 17.24780449347180067, 11.49999999999999645 ) ) ;
#87085=ORIENTED_EDGE ( 'NONE', *, *, #18957, .T. ) ;
#87086=CARTESIAN_POINT ( 'NONE',  ( -99.93377387090225739, -25.31296416273143279, 4.577608519080482274 ) ) ;
#87088=CARTESIAN_POINT ( 'NONE',  ( -109.6228709571501128, -23.95044443724993144, 10.65354141964649592 ) ) ;
#87089=CARTESIAN_POINT ( 'NONE',  ( -26.66703638657053688, -24.80367924758092002, 2.752295699766668324 ) ) ;
#87090=VECTOR ( 'NONE', #28637, 1000.000000000000114 ) ;
#87092=CARTESIAN_POINT ( 'NONE',  ( -50.62287095715005592, -25.00158670708909625, 2.256160236439165967 ) ) ;
#87094=ORIENTED_EDGE ( 'NONE', *, *, #76680, .T. ) ;
#87095=CARTESIAN_POINT ( 'NONE',  ( 19.40787663092975279, -12.54570180764831377, 11.49999999999999645 ) ) ;
#87096=CARTESIAN_POINT ( 'NONE',  ( -22.57016884136470125, -3.422276288085174478, 11.49999999999998934 ) ) ;
#87097=FACE_OUTER_BOUND ( 'NONE', #73586, .T. ) ;
#87098=CARTESIAN_POINT ( 'NONE',  ( -96.51590239563874718, -23.96119346886881019, -0.6495511937832061378 ) ) ;
#87099=CARTESIAN_POINT ( 'NONE',  ( -63.58765420552874303, -24.35071581493543036, 9.817618358456027039 ) ) ;
#87100=CARTESIAN_POINT ( 'NONE',  ( 19.77564376705174709, 10.73071584254150856, 11.49999999999999645 ) ) ;
#87101=ORIENTED_EDGE ( 'NONE', *, *, #49918, .F. ) ;
#87102=CARTESIAN_POINT ( 'NONE',  ( -43.59363013195762449, -24.15543982623907127, -0.2315651400026568496 ) ) ;
#87103=CARTESIAN_POINT ( 'NONE',  ( 19.17116566557315949, -10.70166234769870961, 11.49999999999998934 ) ) ;
#87104=CARTESIAN_POINT ( 'NONE',  ( -114.5228709571500616, -23.47596703998600631, 11.44779298504228038 ) ) ;
#87105=CARTESIAN_POINT ( 'NONE',  ( -44.60008577590918577, -23.96169478059712787, 10.65365249895718414 ) ) ;
#87106=CARTESIAN_POINT ( 'NONE',  ( -69.00489863181175565, -25.19577062647930177, 6.635084460666881512 ) ) ;
#87108=CARTESIAN_POINT ( 'NONE',  ( -92.55620429048340725, -24.64898659630529210, 1.056161002820829919 ) ) ;
#87110=ORIENTED_EDGE ( 'NONE', *, *, #15111, .F. ) ;
#87111=EDGE_CURVE ( 'NONE', #38526, #61427, #69738, .T. ) ;
#87112=CARTESIAN_POINT ( 'NONE',  ( -5.951451697817415010, -19.63005813332872762, 11.49999999999998934 ) ) ;
#87113=ORIENTED_EDGE ( 'NONE', *, *, #61204, .F. ) ;
#87114=ORIENTED_EDGE ( 'NONE', *, *, #69014, .T. ) ;
#87116=ORIENTED_EDGE ( 'NONE', *, *, #4444, .F. ) ;
#87117=CARTESIAN_POINT ( 'NONE',  ( 8.651921485055520833, -21.43433228965458781, 11.49999999999998934 ) ) ;
#87118=CARTESIAN_POINT ( 'NONE',  ( -41.52287095715005449, -23.73934037231755667, 11.05740245334329686 ) ) ;
#87119=CARTESIAN_POINT ( 'NONE',  ( -16.58479117878708209, 11.75282063728064053, -1.500000000000002220 ) ) ;
#87124=CARTESIAN_POINT ( 'NONE',  ( -38.52287095715006870, -29.50250243563736774, 8.947779886222148704 ) ) ;
#87126=CARTESIAN_POINT ( 'NONE',  ( -114.6228709571500559, -24.66019654487199730, 8.947790411086122830 ) ) ;
#87128=CARTESIAN_POINT ( 'NONE',  ( -8.943896628894790979, 19.53434260886740503, 11.49999999999999645 ) ) ;
#87129=ORIENTED_EDGE ( 'NONE', *, *, #64830, .T. ) ;
#87130=CARTESIAN_POINT ( 'NONE',  ( -125.5228709571500616, -24.99132157543084531, 2.256160258750667502 ) ) ;
#87131=CARTESIAN_POINT ( 'NONE',  ( -49.69311491917191148, -25.31573826004878569, 4.912235031306626531 ) ) ;
#87132=ADVANCED_FACE ( 'NONE', ( #18938 ), #72244, .F. ) ;
#87133=ORIENTED_EDGE ( 'NONE', *, *, #70845, .T. ) ;
#87134=EDGE_CURVE ( 'NONE', #58829, #91753, #30421, .T. ) ;
#87135=CARTESIAN_POINT ( 'NONE',  ( -1.268444833121266546, 20.69640364028325052, 11.49999999999998934 ) ) ;
#87136=EDGE_LOOP ( 'NONE', ( #3285, #94240, #6638, #58677 ) ) ;
#87137=CARTESIAN_POINT ( 'NONE',  ( -125.6234887985724953, -25.00158670708911046, 2.256160236439218369 ) ) ;
#87140=CARTESIAN_POINT ( 'NONE',  ( -77.52287095715004739, -23.94994826722564696, -0.6494450866342714734 ) ) ;
#87142=ORIENTED_EDGE ( 'NONE', *, *, #67143, .T. ) ;
#87145=DIRECTION ( 'NONE',  ( 0.000000000000000000, -0.9999999999976377785, -2.173523156925979128E-06 ) ) ;
#87147=CARTESIAN_POINT ( 'NONE',  ( -29.81175120719462512, -25.25636103033882307, 4.942810967025194735 ) ) ;
#87148=CARTESIAN_POINT ( 'NONE',  ( -0.4018715335629812202, -22.01094342083549193, 11.49999999999999645 ) ) ;
#87150=CARTESIAN_POINT ( 'NONE',  ( -103.5477577631356354, -24.65952944569305316, 1.056160979905703234 ) ) ;
#87151=CARTESIAN_POINT ( 'NONE',  ( 11.79716412695777272, 19.27136520130675024, 11.49999999999998934 ) ) ;
#87153=CARTESIAN_POINT ( 'NONE',  ( 14.98681507544721292, -14.71779577663021321, 11.49999999999998934 ) ) ;
#87156=ORIENTED_EDGE ( 'NONE', *, *, #95826, .T. ) ;
#87159=DIRECTION ( 'NONE',  ( -0.000000000000000000, 2.173523156925979552E-06, -0.9999999999976378895 ) ) ;
#87160=ORIENTED_EDGE ( 'NONE', *, *, #78625, .F. ) ;
#87161=CARTESIAN_POINT ( 'NONE',  ( 8.100108036306837178, -19.54698220168213041, 11.49999999999998934 ) ) ;
#87163=CARTESIAN_POINT ( 'NONE',  ( -51.90898564286461436, -25.03148495602775725, 6.429377976798327232 ) ) ;
#87165=CARTESIAN_POINT ( 'NONE',  ( -125.6228709571500275, -23.84047902841601640, -0.8780736468305819775 ) ) ;
#87167=CARTESIAN_POINT ( 'NONE',  ( 20.56832688555235222, -8.368550285707721414, -1.500000000000002220 ) ) ;
#87168=CARTESIAN_POINT ( 'NONE',  ( -114.5873130560532900, -24.65952944569305316, 1.056160979905706343 ) ) ;
#87169=B_SPLINE_CURVE_WITH_KNOTS ( 'NONE', 3,
 ( #39126, #31516, #23384, #86307, #92907, #16792 ),
 .UNSPECIFIED., .F., .F.,
 ( 4, 2, 4 ),
 ( 6.391158118952235087E-06, 0.001387004593080770317, 0.002767618028042588118 ),
 .UNSPECIFIED. ) ;
#87170=EDGE_CURVE ( 'NONE', #76269, #33339, #57527, .T. ) ;
#87173=CARTESIAN_POINT ( 'NONE',  ( -48.62287095715004881, -23.72747288104441310, -1.053458166803663332 ) ) ;
#87174=CARTESIAN_POINT ( 'NONE',  ( -17.66094656686658482, 7.961706694365092041, 11.49999999999999645 ) ) ;
#87175=CARTESIAN_POINT ( 'NONE',  ( -122.6228709571500417, -29.50248528299804818, 1.056150453629045360 ) ) ;
#87177=CARTESIAN_POINT ( 'NONE',  ( -8.384790838521158918, 17.58144419890746235, 11.49999999999998934 ) ) ;
#87178=CARTESIAN_POINT ( 'NONE',  ( -5.333777546869826303, -20.73983961313815172, 11.49999999999998934 ) ) ;
#87179=CARTESIAN_POINT ( 'NONE',  ( -85.52287095715006160, -24.82576562948883492, 8.398263436605596155 ) ) ;
#87181=CARTESIAN_POINT ( 'NONE',  ( -51.65966576824040146, -23.48783264082476308, -1.443836473390094133 ) ) ;
#87182=CARTESIAN_POINT ( 'NONE',  ( -52.62287095715005592, -29.50248528299804818, 1.056150453629033370 ) ) ;
#87183=CARTESIAN_POINT ( 'NONE',  ( -2.506051680461856890, -22.62920675306992280, -1.500000000000002220 ) ) ;
#87184=EDGE_CURVE ( 'NONE', #65117, #80623, #35296, .T. ) ;
#87186=DIRECTION ( 'NONE',  ( -1.000000000000000000, -3.773278334444167608E-23, -8.201307833595939069E-29 ) ) ;
#87187=CARTESIAN_POINT ( 'NONE',  ( -98.62287095715004170, -23.73907113216990794, -1.053371485793225704 ) ) ;
#87188=CARTESIAN_POINT ( 'NONE',  ( -19.77004505525285083, 2.005399880840008642, 11.49999999999999645 ) ) ;
#87194=EDGE_CURVE ( 'NONE', #5560, #43445, #94576, .T. ) ;
#87195=CARTESIAN_POINT ( 'NONE',  ( -80.52287095715007581, -24.14406661686764366, 10.28769366194071821 ) ) ;
#87197=CARTESIAN_POINT ( 'NONE',  ( -20.76051858633888259, -6.224802954461835292, -1.500000000000002220 ) ) ;
#87198=CARTESIAN_POINT ( 'NONE',  ( -56.61228501525301482, -23.48786465467241413, 11.44779295918254647 ) ) ;
#87199=CARTESIAN_POINT ( 'NONE',  ( 4.201609111248720829, -18.99613120386805676, -1.500000000000002220 ) ) ;
#87201=VERTEX_POINT ( 'NONE', #56526 ) ;
#87202=CARTESIAN_POINT ( 'NONE',  ( -10.01004151551622456, -17.79114453763541093, 11.49999999999999645 ) ) ;
#87203=CARTESIAN_POINT ( 'NONE',  ( -49.52287095715006160, -23.47596703998600631, 11.44779298504229104 ) ) ;
#87209=CARTESIAN_POINT ( 'NONE',  ( -39.06913928595307084, -25.31628511282779925, 4.503859277642591863 ) ) ;
#87214=CARTESIAN_POINT ( 'NONE',  ( -66.62726695432588997, -24.51419770103157347, 9.386484678747176957 ) ) ;
#87216=CARTESIAN_POINT ( 'NONE',  ( -9.034649315346676701, 21.08484869742704504, 11.49999999999999645 ) ) ;
#87217=CARTESIAN_POINT ( 'NONE',  ( 22.46337926046256328, 3.617889471270266277, -1.500000000000002220 ) ) ;
#87218=ORIENTED_EDGE ( 'NONE', *, *, #62982, .T. ) ;
#87219=CARTESIAN_POINT ( 'NONE',  ( -110.5116820962086592, -24.83644354573579349, 8.397322867130096569 ) ) ;
#87220=CARTESIAN_POINT ( 'NONE',  ( -98.52287095715001897, -24.34917612406837151, 0.1852690917426555450 ) ) ;
#87221=CARTESIAN_POINT ( 'NONE',  ( -123.5562042904833788, -24.66019654487199730, 8.947790411086119278 ) ) ;
#87222=CARTESIAN_POINT ( 'NONE',  ( -73.52287095715010423, -23.48783264082477018, -1.443836473390093689 ) ) ;
#87223=B_SPLINE_CURVE_WITH_KNOTS ( 'NONE', 3,
 ( #29032, #60511, #90936, #91425 ),
 .UNSPECIFIED., .F., .F.,
 ( 4, 4 ),
 ( 0.000000000000000000, 9.999999999998897304E-05 ),
 .UNSPECIFIED. ) ;
#87224=CARTESIAN_POINT ( 'NONE',  ( -74.52287095715006160, -24.50216790748204687, 0.6166512839542546143 ) ) ;
#87225=CARTESIAN_POINT ( 'NONE',  ( -27.61288548982546232, -24.76667042481958703, 2.278808687314067161 ) ) ;
#87229=CARTESIAN_POINT ( 'NONE',  ( 4.102729645046709450, 19.96921287702725323, 11.49999999999998934 ) ) ;
#87230=EDGE_LOOP ( 'NONE', ( #83742, #68086, #20745, #38054 ) ) ;
#87232=CARTESIAN_POINT ( 'NONE',  ( -22.84742429131147645, -2.885717679200183738, -1.500000000000002220 ) ) ;
#87233=CARTESIAN_POINT ( 'NONE',  ( -99.62287095715004170, -24.66019654487199730, 8.947790411086122830 ) ) ;
#87234=ORIENTED_EDGE ( 'NONE', *, *, #86913, .F. ) ;
#87236=CARTESIAN_POINT ( 'NONE',  ( -101.5228709571500758, -23.72747288104470087, -1.053458166803225460 ) ) ;
#87237=B_SPLINE_CURVE_WITH_KNOTS ( 'NONE', 3,
 ( #16034, #821, #31774, #76428 ),
 .UNSPECIFIED., .F., .F.,
 ( 4, 4 ),
 ( 0.8704074611401169115, 0.8794138924122323342 ),
 .UNSPECIFIED. ) ;
#87238=CARTESIAN_POINT ( 'NONE',  ( -95.59855702225377172, -23.85016227208581086, -0.8807180028928282001 ) ) ;
#87239=CARTESIAN_POINT ( 'NONE',  ( -29.55620429048340725, -24.57875649265860574, 1.056161290661043584 ) ) ;
#87240=VECTOR ( 'NONE', #67257, 1000.000000000000114 ) ;
#87241=CARTESIAN_POINT ( 'NONE',  ( -20.89022842043660688, 4.291957016416017900, 11.49999999999999645 ) ) ;
#87243=EDGE_CURVE ( 'NONE', #49692, #83380, #89736, .T. ) ;
#87245=CARTESIAN_POINT ( 'NONE',  ( 10.78255534502030777, 19.45608938089507234, 11.49999999999998934 ) ) ;
#87246=EDGE_CURVE ( 'NONE', #22752, #64178, #34966, .T. ) ;
#87247=CARTESIAN_POINT ( 'NONE',  ( 14.37238272058661259, 14.81585024043302035, -1.500000000000002220 ) ) ;
#87248=VERTEX_POINT ( 'NONE', #55424 ) ;
#87250=CARTESIAN_POINT ( 'NONE',  ( -56.62287095715005592, -23.48783264082478084, -1.443836473390068820 ) ) ;
#87251=EDGE_LOOP ( 'NONE', ( #59823, #19215, #38238, #26855 ) ) ;
#87252=CARTESIAN_POINT ( 'NONE',  ( -95.52287095715004739, -24.62226745350443124, 0.9660975649729501846 ) ) ;
#87254=CARTESIAN_POINT ( 'NONE',  ( -58.55986427732528199, -23.73791477778912196, 11.05961554403170588 ) ) ;
#87256=CARTESIAN_POINT ( 'NONE',  ( 17.92008016455634589, 10.74458801173053324, -1.500000000000002220 ) ) ;
#87258=CARTESIAN_POINT ( 'NONE',  ( 12.52028139621776326, 17.89958603277719718, 11.49999999999999645 ) ) ;
#87261=CARTESIAN_POINT ( 'NONE',  ( 0.003324065884441271702, 22.49086686382009503, 11.49999999999998934 ) ) ;
#87262=CARTESIAN_POINT ( 'NONE',  ( -8.544475976622297964, 19.10969517993760292, -1.500000000000002220 ) ) ;
#87263=CARTESIAN_POINT ( 'NONE',  ( -62.52287095715006160, -24.64898659630367561, 1.056161002820822592 ) ) ;
#87266=ORIENTED_EDGE ( 'NONE', *, *, #4430, .F. ) ;
#87267=ORIENTED_EDGE ( 'NONE', *, *, #57693, .F. ) ;
#87269=CARTESIAN_POINT ( 'NONE',  ( -52.58733020142698678, -24.34968618360933945, 0.1864209137778880532 ) ) ;
#87271=CARTESIAN_POINT ( 'NONE',  ( 16.24497012180664868, 13.92215130028523973, -1.500000000000002220 ) ) ;
#87272=CARTESIAN_POINT ( 'NONE',  ( -13.11617634606977489, 18.14055439154125438, 11.49999999999999645 ) ) ;
#87275=CARTESIAN_POINT ( 'NONE',  ( 20.41947327098772647, -5.118016103960565388, 11.49999999999998934 ) ) ;
#87276=CARTESIAN_POINT ( 'NONE',  ( -30.42977181688026533, -24.56940358145610048, 9.174392229302920754 ) ) ;
#87277=CARTESIAN_POINT ( 'NONE',  ( -2.986242917674419850, -19.73498743542299749, -1.500000000000002220 ) ) ;
#87279=CARTESIAN_POINT ( 'NONE',  ( -101.5105966293721877, -24.51314013834316086, 0.6176544820404185065 ) ) ;
#87280=CARTESIAN_POINT ( 'NONE',  ( -17.89045161427552699, -12.92718102017995641, -1.500000000000002220 ) ) ;
#87281=ORIENTED_EDGE ( 'NONE', *, *, #79212, .T. ) ;
#87282=B_SPLINE_CURVE_WITH_KNOTS ( 'NONE', 3,
 ( #58080, #28112, #20977, #35728, #42851, #65699, #96613, #4773, #34232, #65205, #26615, #50957 ),
 .UNSPECIFIED., .F., .F.,
 ( 4, 2, 2, 2, 2, 4 ),
 ( 0.000000000000000000, 0.0003036893844903788245, 0.0006073787689807576490, 0.0009110681534711365277, 0.001062912845716322335, 0.001214757537961508359 ),
 .UNSPECIFIED. ) ;
#87283=CARTESIAN_POINT ( 'NONE',  ( -65.62787617961251385, -24.83644354573579349, 8.397322867130094792 ) ) ;
#87284=DIRECTION ( 'NONE',  ( -3.773278334453079618E-23, 0.9999999999976377785, 2.173523156925979975E-06 ) ) ;
#87285=CARTESIAN_POINT ( 'NONE',  ( 4.135342931496230001, -20.44547621892628797, 11.49999999999999645 ) ) ;
#87287=ADVANCED_FACE ( 'NONE', ( #12620 ), #57818, .T. ) ;
#87288=CARTESIAN_POINT ( 'NONE',  ( -47.52287095715007581, -23.72747288104469732, -1.053458166803227236 ) ) ;
#87289=CARTESIAN_POINT ( 'NONE',  ( -25.57936158321581033, -24.88095430358513838, 4.018852390678397057 ) ) ;
#87290=AXIS2_PLACEMENT_3D ( 'NONE', #79332, #48904, #47899 ) ;
#87291=CARTESIAN_POINT ( 'NONE',  ( -117.5228709571500474, -24.51283580621365843, 0.6167428607019750375 ) ) ;
#87292=CARTESIAN_POINT ( 'NONE',  ( -13.37813101364405100, 16.61575060780308277, -1.500000000000002220 ) ) ;
#87295=ADVANCED_FACE ( 'NONE', ( #86853 ), #4020, .T. ) ;
#87296=CARTESIAN_POINT ( 'NONE',  ( -83.62287095715005592, -23.48783264082478794, -1.443836473390065711 ) ) ;
#87298=CARTESIAN_POINT ( 'NONE',  ( 1.525329354412473970, -22.51392980886878448, -1.500000000000002220 ) ) ;
#87300=EDGE_LOOP ( 'NONE', ( #51593, #33202, #87405, #98587 ) ) ;
#87301=CARTESIAN_POINT ( 'NONE',  ( -111.3776484685884327, -29.50249240399202222, 4.332395270848422797 ) ) ;
#87303=CARTESIAN_POINT ( 'NONE',  ( 3.669390655483735220, -19.36157329643844704, 11.49999999999999645 ) ) ;
#87304=CARTESIAN_POINT ( 'NONE',  ( -32.52287095715004739, -23.47593901973090169, -1.443836447538997092 ) ) ;
#87305=AXIS2_PLACEMENT_3D ( 'NONE', #96326, #35435, #95822 ) ;
#87306=B_SPLINE_CURVE_WITH_KNOTS ( 'NONE', 3,
 ( #96952, #52281, #44171, #98432, #36544, #21806 ),
 .UNSPECIFIED., .F., .F.,
 ( 4, 2, 4 ),
 ( 0.000000000000000000, 0.001380764517853250552, 0.002761529035706501104 ),
 .UNSPECIFIED. ) ;
#87309=CARTESIAN_POINT ( 'NONE',  ( -89.52287095715006160, -23.47596703998600631, 11.44779298504228393 ) ) ;
#87311=CARTESIAN_POINT ( 'NONE',  ( -124.5569032301564363, -23.48786465467241769, 11.44779295918253581 ) ) ;
#87312=CARTESIAN_POINT ( 'NONE',  ( -76.62287095715007013, -24.64898659630367916, 1.056161002820826145 ) ) ;
#87314=DIRECTION ( 'NONE',  ( 1.000000000000000000, 3.773278334444167608E-23, 8.201307833595939069E-29 ) ) ;
#87315=CARTESIAN_POINT ( 'NONE',  ( 6.816645498261984848, 18.52099371530728789, 11.49999999999998934 ) ) ;
#87316=ORIENTED_EDGE ( 'NONE', *, *, #51205, .F. ) ;
#87317=CARTESIAN_POINT ( 'NONE',  ( 16.36621611169882229, 11.82581248522330064, 11.49999999999999645 ) ) ;
#87319=EDGE_CURVE ( 'NONE', #43640, #45268, #58314, .T. ) ;
#87321=ORIENTED_EDGE ( 'NONE', *, *, #14979, .T. ) ;
#87323=CARTESIAN_POINT ( 'NONE',  ( -41.62287095715006302, -23.47596703998600276, 11.44779298504227505 ) ) ;
#87325=CARTESIAN_POINT ( 'NONE',  ( -82.62287095715005592, -23.72747288104469376, -1.053458166803226792 ) ) ;
#87327=CARTESIAN_POINT ( 'NONE',  ( -81.55620429048340725, -24.65952944569304606, 1.056160979905699238 ) ) ;
#87328=CARTESIAN_POINT ( 'NONE',  ( -19.63739455291241498, 3.909132673056371132, -1.500000000000002220 ) ) ;
#87330=DIRECTION ( 'NONE',  ( 3.773278334444166432E-23, -1.000000000000000000, 0.000000000000000000 ) ) ;
#87332=EDGE_CURVE ( 'NONE', #75504, #98076, #34024, .T. ) ;
#87333=CARTESIAN_POINT ( 'NONE',  ( -79.63359060245308285, -24.15620529776628089, 10.23563542870660470 ) ) ;
#87335=DIRECTION ( 'NONE',  ( -1.000000000000000000, -3.773278334444166432E-23, -8.201307841325785021E-29 ) ) ;
#87336=CARTESIAN_POINT ( 'NONE',  ( -38.52287095715008292, -23.48783264083452593, -1.443836473374935592 ) ) ;
#87337=CARTESIAN_POINT ( 'NONE',  ( -73.51656568446136930, -23.73766607897670511, -1.055555164236457344 ) ) ;
#87338=DIRECTION ( 'NONE',  ( -3.773278334453080206E-23, 0.9999999999976377785, 2.173523156925979975E-06 ) ) ;
#87339=DIRECTION ( 'NONE',  ( 0.000000000000000000, -0.9999999999976377785, -2.173523156925979975E-06 ) ) ;
#87341=AXIS2_PLACEMENT_3D ( 'NONE', #28316, #83591, #28820 ) ;
#87343=CARTESIAN_POINT ( 'NONE',  ( 20.05691770114479766, 3.104179615465487707, -1.500000000000002220 ) ) ;
#87346=B_SPLINE_CURVE_WITH_KNOTS ( 'NONE', 3,
 ( #63612, #70701, #85417, #1199, #9802, #86921 ),
 .UNSPECIFIED., .F., .F.,
 ( 4, 2, 4 ),
 ( 0.000000000000000000, 0.001380764517854764098, 0.002761529035709528197 ),
 .UNSPECIFIED. ) ;
#87347=CARTESIAN_POINT ( 'NONE',  ( -109.5228709571500474, -23.48783264082477018, -1.443836473390083253 ) ) ;
#87348=CARTESIAN_POINT ( 'NONE',  ( -127.5894455380119865, -24.51419770103158768, 9.386484678747160970 ) ) ;
#87350=CARTESIAN_POINT ( 'NONE',  ( -88.62287095715004170, -23.48786465467241769, 11.44779295918254114 ) ) ;
#87351=CARTESIAN_POINT ( 'NONE',  ( -81.62287095715007013, -23.73907113216990794, -1.053371485793228368 ) ) ;
#87352=CARTESIAN_POINT ( 'NONE',  ( -30.47287095715006444, -24.91388280771538533, 8.081096783492887070 ) ) ;
#87353=CARTESIAN_POINT ( 'NONE',  ( -6.202713861520617655, -20.23501359363181962, 11.49999999999999645 ) ) ;
#87354=B_SPLINE_CURVE_WITH_KNOTS ( 'NONE', 3,
 ( #73959, #3461, #43514, #42525 ),
 .UNSPECIFIED., .F., .F.,
 ( 4, 4 ),
 ( 0.000000000000000000, 9.999999999998897304E-05 ),
 .UNSPECIFIED. ) ;
#87356=CARTESIAN_POINT ( 'NONE',  ( 21.55033589006239936, 5.121329677682045833, -1.500000000000002220 ) ) ;
#87358=CARTESIAN_POINT ( 'NONE',  ( -18.72588118538106272, -8.511115862834014223, 11.49999999999998934 ) ) ;
#87360=CARTESIAN_POINT ( 'NONE',  ( -88.52287095715009002, -23.48783264082477018, -1.443836473390089692 ) ) ;
#87361=ORIENTED_EDGE ( 'NONE', *, *, #53700, .T. ) ;
#87362=EDGE_CURVE ( 'NONE', #44716, #62727, #74028, .T. ) ;
#87363=FACE_OUTER_BOUND ( 'NONE', #36670, .T. ) ;
#87364=CARTESIAN_POINT ( 'NONE',  ( -70.52287095715009002, -24.62285846331437256, 9.038163153548294915 ) ) ;
#87365=ORIENTED_EDGE ( 'NONE', *, *, #38202, .F. ) ;
#87366=EDGE_LOOP ( 'NONE', ( #97016, #26723, #98634, #45569 ) ) ;
#87369=CARTESIAN_POINT ( 'NONE',  ( -117.5228709571500758, -23.47593901973090524, -1.443836447538996204 ) ) ;
#87370=CARTESIAN_POINT ( 'NONE',  ( -80.62287095715005592, -29.50250786944525672, 11.44777988621623521 ) ) ;
#87372=CARTESIAN_POINT ( 'NONE',  ( -17.23291202157775359, 11.51834372740795231, -1.500000000000002220 ) ) ;
#87373=EDGE_CURVE ( 'NONE', #62610, #55233, #97364, .T. ) ;
#87374=CARTESIAN_POINT ( 'NONE',  ( -21.36891742734480104, 3.643610035731704055, 11.49999999999999645 ) ) ;
#87375=ORIENTED_EDGE ( 'NONE', *, *, #53589, .F. ) ;
#87376=CARTESIAN_POINT ( 'NONE',  ( -127.5562042904834215, -24.65952944569304606, 1.056160979905708563 ) ) ;
#87378=CARTESIAN_POINT ( 'NONE',  ( -3.217810451210200817, -22.18463865543611391, 11.49999999999998934 ) ) ;
#87379=ADVANCED_FACE ( 'NONE', ( #6005 ), #59304, .T. ) ;
#87380=CARTESIAN_POINT ( 'NONE',  ( -47.60695248165256288, -23.73791477778911485, 11.05961554403170766 ) ) ;
#87381=CARTESIAN_POINT ( 'NONE',  ( -123.5228709571500616, -24.65952944569304961, 1.056160979905705899 ) ) ;
#87387=CARTESIAN_POINT ( 'NONE',  ( -45.52287095715006870, -23.84081130425358097, 10.88220057483157888 ) ) ;
#87388=ORIENTED_EDGE ( 'NONE', *, *, #69839, .T. ) ;
#87390=B_SPLINE_CURVE_WITH_KNOTS ( 'NONE', 3,
 ( #54453, #46842, #16881, #62571, #39214, #100092 ),
 .UNSPECIFIED., .F., .F.,
 ( 4, 2, 4 ),
 ( 6.391158118972359742E-06, 0.001387004593080787881, 0.002767618028042603297 ),
 .UNSPECIFIED. ) ;
#87392=CARTESIAN_POINT ( 'NONE',  ( 12.26186175617451113, -17.30295086655154080, -1.500000000000002220 ) ) ;
#87395=B_SPLINE_CURVE_WITH_KNOTS ( 'NONE', 3,
 ( #6692, #38137, #83313, #22892 ),
 .UNSPECIFIED., .F., .F.,
 ( 4, 4 ),
 ( 0.000000000000000000, 9.999999999998900014E-05 ),
 .UNSPECIFIED. ) ;
#87396=CARTESIAN_POINT ( 'NONE',  ( -15.04333773895388937, -15.80532200100455498, -1.500000000000002220 ) ) ;
#87397=CARTESIAN_POINT ( 'NONE',  ( -52.54748251683253102, -24.15620529776627734, 10.23563542870661180 ) ) ;
#87400=CARTESIAN_POINT ( 'NONE',  ( 8.176594470695947692, -20.27425322898990601, -1.500000000000002220 ) ) ;
#87402=EDGE_LOOP ( 'NONE', ( #78717, #69046, #16480, #5620 ) ) ;
#87403=DIRECTION ( 'NONE',  ( 0.000000000000000000, 0.9999999999976377785, 2.173523156925979552E-06 ) ) ;
#87404=CARTESIAN_POINT ( 'NONE',  ( -85.55305756195892286, -24.15602025860895807, 10.28564288303535967 ) ) ;
#87405=ORIENTED_EDGE ( 'NONE', *, *, #56463, .T. ) ;
#87406=B_SPLINE_CURVE_WITH_KNOTS ( 'NONE', 3,
 ( #15416, #16923, #63623, #93037, #32646, #22518, #69724, #69214 ),
 .UNSPECIFIED., .F., .F.,
 ( 4, 2, 2, 4 ),
 ( 6.391158118970574197E-06, 0.002007136338672929621, 0.003007508928949906898, 0.004007881519226884175 ),
 .UNSPECIFIED. ) ;
#87407=VERTEX_POINT ( 'NONE', #99831 ) ;
#87408=ORIENTED_EDGE ( 'NONE', *, *, #80306, .T. ) ;
#87409=FACE_OUTER_BOUND ( 'NONE', #99784, .T. ) ;
#87410=CARTESIAN_POINT ( 'NONE',  ( -82.58520315302067161, -24.51314013834315375, 0.6176544820404169522 ) ) ;
#87411=CARTESIAN_POINT ( 'NONE',  ( -19.96038302963917488, -7.207760892512529161, 11.49999999999998934 ) ) ;
#87413=CARTESIAN_POINT ( 'NONE',  ( -130.5728709571500588, -24.14929313691198232, 10.49653219292474482 ) ) ;
#87416=CARTESIAN_POINT ( 'NONE',  ( 3.148799746435844593, 19.17640706095922098, -1.500000000000002220 ) ) ;
#87418=CARTESIAN_POINT ( 'NONE',  ( -80.58953762381671027, -23.48786465467241058, 11.44779295918254469 ) ) ;
#87419=ORIENTED_EDGE ( 'NONE', *, *, #8107, .T. ) ;
#87420=CARTESIAN_POINT ( 'NONE',  ( 19.19537281719634336, 3.394423509666608663, 11.49999999999999645 ) ) ;
#87422=VECTOR ( 'NONE', #38672, 1000.000000000000114 ) ;
#87424=ORIENTED_EDGE ( 'NONE', *, *, #60925, .F. ) ;
#87426=FACE_OUTER_BOUND ( 'NONE', #74970, .T. ) ;
#87428=CARTESIAN_POINT ( 'NONE',  ( -80.55620429048342146, -23.47596703998600276, 11.44779298504227683 ) ) ;
#87430=CARTESIAN_POINT ( 'NONE',  ( -10.66912846187372210, -16.51573522771486324, -1.500000000000002220 ) ) ;
#87432=ORIENTED_EDGE ( 'NONE', *, *, #9737, .T. ) ;
#87434=B_SPLINE_CURVE_WITH_KNOTS ( 'NONE', 3,
 ( #20964, #59054, #90488, #74754 ),
 .UNSPECIFIED., .F., .F.,
 ( 4, 4 ),
 ( 0.000000000000000000, 0.0001000000000000028644 ),
 .UNSPECIFIED. ) ;
#87435=DIRECTION ( 'NONE',  ( 0.000000000000000000, -0.9999999999976377785, -2.173523156925979975E-06 ) ) ;
#87436=CARTESIAN_POINT ( 'NONE',  ( -21.10450430117995424, 9.351148110661185342, -1.500000000000002220 ) ) ;
#87437=EDGE_CURVE ( 'NONE', #79765, #17650, #90248, .T. ) ;
#87441=CARTESIAN_POINT ( 'NONE',  ( -60.52287095715006160, -23.47596703998600631, 11.44779298504228926 ) ) ;
#87442=CARTESIAN_POINT ( 'NONE',  ( -109.8778697195837992, -25.12043765296585818, 2.888617715527074470 ) ) ;
#87443=CARTESIAN_POINT ( 'NONE',  ( -97.54779265495582763, -24.51419770103157703, 9.386484678747176957 ) ) ;
#87444=FACE_OUTER_BOUND ( 'NONE', #40754, .T. ) ;
#87446=CARTESIAN_POINT ( 'NONE',  ( -44.52287095715009713, -23.96127896941631619, -0.6493128931038062435 ) ) ;
#87447=PLANE ( 'NONE',  #70020 ) ;
#87448=CARTESIAN_POINT ( 'NONE',  ( -114.6307875202147812, -23.48786465467241769, 11.44779295918253759 ) ) ;
#87449=CARTESIAN_POINT ( 'NONE',  ( 1.402406813841059030, 19.88454085074057076, -1.500000000000002220 ) ) ;
#87450=FACE_OUTER_BOUND ( 'NONE', #13368, .T. ) ;
#87451=EDGE_CURVE ( 'NONE', #98355, #18610, #32751, .T. ) ;
#87452=CARTESIAN_POINT ( 'NONE',  ( -1.769646468872753120, 19.80360307839763934, -1.500000000000002220 ) ) ;
#87455=CARTESIAN_POINT ( 'NONE',  ( -29.52287095715004739, -24.41831317116936262, 0.6165372783097629039 ) ) ;
#87457=ADVANCED_FACE ( 'NONE', ( #21713 ), #99345, .F. ) ;
#87460=CARTESIAN_POINT ( 'NONE',  ( -3.686900873480770002, -20.48319827837541141, 11.49999999999999645 ) ) ;
#87461=CARTESIAN_POINT ( 'NONE',  ( -81.64115287866665938, -23.73766607897671221, -1.055555164236432919 ) ) ;
#87462=CARTESIAN_POINT ( 'NONE',  ( -75.62287095715004170, -24.99156045073392818, 7.747789690856161648 ) ) ;
#87463=CARTESIAN_POINT ( 'NONE',  ( 22.20583189720066741, -5.198064566299082756, 11.49999999999999645 ) ) ;
#87464=ORIENTED_EDGE ( 'NONE', *, *, #54601, .F. ) ;
#87465=CARTESIAN_POINT ( 'NONE',  ( -56.52287095715006870, -29.50248528299804818, 1.056150453629034924 ) ) ;
#87468=CARTESIAN_POINT ( 'NONE',  ( -18.82339984186270598, 7.397194320553815317, -1.500000000000002220 ) ) ;
#87469=B_SPLINE_CURVE_WITH_KNOTS ( 'NONE', 3,
 ( #23701, #29321, #21693, #38435 ),
 .UNSPECIFIED., .F., .F.,
 ( 4, 4 ),
 ( 0.000000000000000000, 0.0001000000000000167422 ),
 .UNSPECIFIED. ) ;
#87470=EDGE_CURVE ( 'NONE', #8126, #4386, #4911, .T. ) ;
#87472=CARTESIAN_POINT ( 'NONE',  ( -40.54486904600227604, -25.30535573344747036, 5.077984538006014681 ) ) ;
#87474=ORIENTED_EDGE ( 'NONE', *, *, #20837, .F. ) ;
#87475=CARTESIAN_POINT ( 'NONE',  ( -30.64427850938831099, -23.56000036390796382, 11.50200000000000067 ) ) ;
#87476=CARTESIAN_POINT ( 'NONE',  ( -104.5562042904834072, -23.47596703998600631, 11.44779298504227683 ) ) ;
#87477=CARTESIAN_POINT ( 'NONE',  ( 1.468936567494551593, -19.95401460376903913, -1.500000000000002220 ) ) ;
#87478=CARTESIAN_POINT ( 'NONE',  ( -123.5190373946633429, -24.65952944569305316, 1.056160979905706343 ) ) ;
#87479=CARTESIAN_POINT ( 'NONE',  ( -17.07941033872765146, 12.18221932706078370, 11.49999999999999645 ) ) ;
#87481=CARTESIAN_POINT ( 'NONE',  ( -79.62287095715005592, -24.64965695001468404, 8.947790433994182280 ) ) ;
#87482=CARTESIAN_POINT ( 'NONE',  ( -13.14421341422731260, -17.72855101262432242, -1.500000000000002220 ) ) ;
#87483=VECTOR ( 'NONE', #39661, 1000.000000000000227 ) ;
#87486=ORIENTED_EDGE ( 'NONE', *, *, #95, .T. ) ;
#87488=CARTESIAN_POINT ( 'NONE',  ( -49.50910156767503878, -25.27344905013621101, 3.963068828678178335 ) ) ;
#87489=ADVANCED_FACE ( 'NONE', ( #75505 ), #14612, .F. ) ;
#87491=ORIENTED_EDGE ( 'NONE', *, *, #40213, .T. ) ;
#87493=EDGE_LOOP ( 'NONE', ( #67978, #12199, #84360, #97230 ) ) ;
#87499=CARTESIAN_POINT ( 'NONE',  ( 6.429960413904108663, -19.47341730443774921, -1.500000000000002220 ) ) ;
#87500=ADVANCED_FACE ( 'NONE', ( #5506 ), #29843, .T. ) ;
#87501=EDGE_LOOP ( 'NONE', ( #64102, #21089, #51453, #44087 ) ) ;
#87502=CARTESIAN_POINT ( 'NONE',  ( -126.5228709571500616, -24.65952944569305316, 1.056160979905707675 ) ) ;
#87505=CARTESIAN_POINT ( 'NONE',  ( -64.52287095715006160, -24.64965694238407323, 8.947790433994201820 ) ) ;
#87506=CARTESIAN_POINT ( 'NONE',  ( 2.183928509170398602, -22.20744181112294413, 11.49999999999998934 ) ) ;
#87507=EDGE_CURVE ( 'NONE', #32756, #30205, #59355, .T. ) ;
#87508=CARTESIAN_POINT ( 'NONE',  ( -101.5562042904833788, -24.64965694238575011, 8.947790433994192938 ) ) ;
#87511=EDGE_CURVE ( 'NONE', #80236, #95000, #23022, .T. ) ;
#87513=VECTOR ( 'NONE', #61321, 1000.000000000000114 ) ;
#87514=CARTESIAN_POINT ( 'NONE',  ( -32.07722060962682775, -29.50248914092071928, 2.831113219569932227 ) ) ;
#87516=CARTESIAN_POINT ( 'NONE',  ( 20.84756458399398937, 0.1950554047328266483, 11.49999999999998934 ) ) ;
#87518=B_SPLINE_CURVE_WITH_KNOTS ( 'NONE', 3,
 ( #99125, #76287, #60600, #21995 ),
 .UNSPECIFIED., .F., .F.,
 ( 4, 4 ),
 ( 0.000000000000000000, 9.999999999998897304E-05 ),
 .UNSPECIFIED. ) ;
#87519=CARTESIAN_POINT ( 'NONE',  ( -79.52287095715006160, -24.66019654487199375, 8.947790411086122830 ) ) ;
#87520=ORIENTED_EDGE ( 'NONE', *, *, #63878, .F. ) ;
#87521=ORIENTED_EDGE ( 'NONE', *, *, #95629, .T. ) ;
#87522=AXIS2_PLACEMENT_3D ( 'NONE', #81925, #90529, #21502 ) ;
#87523=LINE ( 'NONE', #48966, #21195 ) ;
#87525=CARTESIAN_POINT ( 'NONE',  ( -19.97109070424261645, 6.737033823242594366, -1.500000000000002220 ) ) ;
#87526=ORIENTED_EDGE ( 'NONE', *, *, #20476, .F. ) ;
#87527=CARTESIAN_POINT ( 'NONE',  ( -110.6228709571500559, -24.99132157543166954, 2.256160258750667502 ) ) ;
#87529=PLANE ( 'NONE',  #10826 ) ;
#87532=CARTESIAN_POINT ( 'NONE',  ( 2.849777056880220982, 21.50153301832798647, -1.500000000000002220 ) ) ;
#87534=CARTESIAN_POINT ( 'NONE',  ( 21.15429367616652101, -6.912965584596229895, 11.49999999999999645 ) ) ;
#87535=ORIENTED_EDGE ( 'NONE', *, *, #54377, .F. ) ;
#87536=CARTESIAN_POINT ( 'NONE',  ( -50.82761139903328029, -25.24728739217141538, 5.269904184087572219 ) ) ;
#87537=DIRECTION ( 'NONE',  ( -3.773278334453079030E-23, 0.9999999999976377785, 2.173523156925979128E-06 ) ) ;
#87538=ORIENTED_EDGE ( 'NONE', *, *, #70450, .F. ) ;
#87539=CARTESIAN_POINT ( 'NONE',  ( -118.6228709571500275, -24.33927499327855415, 9.819080762295808285 ) ) ;
#87543=CARTESIAN_POINT ( 'NONE',  ( 16.68447708738676383, -11.30049470069299922, 11.49999999999998934 ) ) ;
#87545=ORIENTED_EDGE ( 'NONE', *, *, #14157, .T. ) ;
#87546=CARTESIAN_POINT ( 'NONE',  ( -130.5728709571500588, -24.48854083826206463, 0.3146758927689199958 ) ) ;
#87547=CARTESIAN_POINT ( 'NONE',  ( 22.28251467978060063, -2.329348454117679879, -1.500000000000002220 ) ) ;
#87548=ORIENTED_EDGE ( 'NONE', *, *, #83132, .F. ) ;
#87549=ORIENTED_EDGE ( 'NONE', *, *, #65552, .T. ) ;
#87550=CARTESIAN_POINT ( 'NONE',  ( -112.6317049575896334, -23.48786465467241769, 11.44779295918253936 ) ) ;
#87551=CARTESIAN_POINT ( 'NONE',  ( -94.51866276539982437, -23.73791477778911840, 11.05961554403170588 ) ) ;
#87554=CARTESIAN_POINT ( 'NONE',  ( -30.60163303648719690, -24.57143472585066135, 0.8294870405985536044 ) ) ;
#87555=CARTESIAN_POINT ( 'NONE',  ( -9.542874777335924819, 17.09510996321218101, -1.500000000000002220 ) ) ;
#87556=CARTESIAN_POINT ( 'NONE',  ( -46.65379568173771929, -23.73766607897669800, -1.055555164236460008 ) ) ;
#87557=ORIENTED_EDGE ( 'NONE', *, *, #83422, .T. ) ;
#87558=CARTESIAN_POINT ( 'NONE',  ( -5.740839400147730309, 20.75665450205591966, 11.49999999999998934 ) ) ;
#87559=CARTESIAN_POINT ( 'NONE',  ( -128.6234765650372935, -24.65952944569304961, 1.056160979905706787 ) ) ;
#87560=CARTESIAN_POINT ( 'NONE',  ( -71.14319566529317740, -25.25639514997889989, 6.703707704318174088 ) ) ;
#87561=DIRECTION ( 'NONE',  ( -1.000000000000000000, -3.773278334444166432E-23, -8.201307841325785021E-29 ) ) ;
#87563=LINE ( 'NONE', #72849, #94155 ) ;
#87564=CARTESIAN_POINT ( 'NONE',  ( 15.01570752033863165, -17.30494853738164096, -1.500000000000002220 ) ) ;
#87565=EDGE_CURVE ( 'NONE', #89859, #79893, #41206, .T. ) ;
#87567=CARTESIAN_POINT ( 'NONE',  ( -128.5228709571500758, -24.64898659630368627, 1.056161002820834804 ) ) ;
#87568=PLANE ( 'NONE',  #70096 ) ;
#87569=CARTESIAN_POINT ( 'NONE',  ( 4.282148337517553749, -19.64591042314588165, 11.49999999999999645 ) ) ;
#87570=CARTESIAN_POINT ( 'NONE',  ( -110.0261373028301080, -25.28814073874244173, 2.855322185807698254 ) ) ;
#87571=CARTESIAN_POINT ( 'NONE',  ( -119.5228709571500474, -23.47593901973090524, -1.443836447538996204 ) ) ;
#87572=EDGE_CURVE ( 'NONE', #77746, #40606, #74032, .T. ) ;
#87573=CARTESIAN_POINT ( 'NONE',  ( -99.52287095715010423, -24.34917612407053156, 0.1852690917483114930 ) ) ;
#87574=CARTESIAN_POINT ( 'NONE',  ( -126.5895376238167529, -23.47596703998600631, 11.44779298504227683 ) ) ;
#87576=CARTESIAN_POINT ( 'NONE',  ( 19.22361159462649027, -4.937694622890139939, 11.49999999999998934 ) ) ;
#87579=CARTESIAN_POINT ( 'NONE',  ( -8.025172913017740939, -17.94849717234452768, -1.500000000000002220 ) ) ;
#87580=ADVANCED_FACE ( 'NONE', ( #47083 ), #69907, .F. ) ;
#87583=VECTOR ( 'NONE', #21750, 1000.000000000000114 ) ;
#87584=CARTESIAN_POINT ( 'NONE',  ( -58.58953762381672448, -23.48786465467241769, 11.44779295918254824 ) ) ;
#87587=EDGE_CURVE ( 'NONE', #60599, #58829, #150, .T. ) ;
#87588=CARTESIAN_POINT ( 'NONE',  ( -60.52287095715004028, -24.14406661686764366, 10.28769366194078216 ) ) ;
#87589=CARTESIAN_POINT ( 'NONE',  ( -39.07220902699673104, -25.29584393180295265, 4.512460029652592297 ) ) ;
#87590=CARTESIAN_POINT ( 'NONE',  ( 10.54205562766345672, -17.70522803435136083, 11.49999999999999645 ) ) ;
#87594=CARTESIAN_POINT ( 'NONE',  ( -21.16596634977960179, 8.012090315382277339, 11.49999999999999645 ) ) ;
#87595=EDGE_LOOP ( 'NONE', ( #45839, #3055, #95635, #92581, #13515, #41452, #34499, #67538 ) ) ;
#87596=CARTESIAN_POINT ( 'NONE',  ( -115.6228709571500417, -23.48783264082478794, -1.443836473390058384 ) ) ;
#87598=CARTESIAN_POINT ( 'NONE',  ( -56.52287095715009002, -23.48783264082476308, -1.443836473390091690 ) ) ;
#87599=CARTESIAN_POINT ( 'NONE',  ( -58.52287095715006160, -29.50247984919015209, -1.443849546365056913 ) ) ;
#87600=ADVANCED_FACE ( 'NONE', ( #17115 ), #91470, .T. ) ;
#87602=CARTESIAN_POINT ( 'NONE',  ( -75.52287095715007581, -23.47593901973090169, -1.443836447538996870 ) ) ;
#87603=ORIENTED_EDGE ( 'NONE', *, *, #74950, .F. ) ;
#87605=CARTESIAN_POINT ( 'NONE',  ( 8.286623624103266097E-13, -23.05000000000000426, 11.49999999999999645 ) ) ;
#87606=CARTESIAN_POINT ( 'NONE',  ( -5.953223121155255981, 22.05028593715628560, 11.49999999999998934 ) ) ;
#87607=FACE_OUTER_BOUND ( 'NONE', #46481, .T. ) ;
#87608=CARTESIAN_POINT ( 'NONE',  ( -96.63278121929289455, -23.96119346886881019, -0.6495511937832062488 ) ) ;
#87609=CARTESIAN_POINT ( 'NONE',  ( -63.49529785725831488, -24.51419770103156992, 9.386484678747175181 ) ) ;
#87610=CARTESIAN_POINT ( 'NONE',  ( -20.52357230491503159, 9.176553703681571861, 11.49999999999999645 ) ) ;
#87611=EDGE_LOOP ( 'NONE', ( #70702, #49614, #13480, #18440 ) ) ;
#87612=DIRECTION ( 'NONE',  ( -3.773278334453079030E-23, 0.9999999999976377785, 2.173523156925979128E-06 ) ) ;
#87613=CARTESIAN_POINT ( 'NONE',  ( -21.26704322615652032, -5.532269525099344776, 11.49999999999998934 ) ) ;
#87614=B_SPLINE_CURVE_WITH_KNOTS ( 'NONE', 3,
 ( #84136, #16127, #4656, #58943 ),
 .UNSPECIFIED., .F., .F.,
 ( 4, 4 ),
 ( 0.9511792137939691916, 0.9601856450660847253 ),
 .UNSPECIFIED. ) ;
#87615=CARTESIAN_POINT ( 'NONE',  ( -54.62287095715005592, -24.65952944569304606, 1.056160979905694131 ) ) ;
#87616=CARTESIAN_POINT ( 'NONE',  ( -34.51265709502276735, -23.73791477778911485, 11.05961554403171299 ) ) ;
#87619=FACE_OUTER_BOUND ( 'NONE', #85343, .T. ) ;
#87620=FACE_OUTER_BOUND ( 'NONE', #70403, .T. ) ;
#87622=CARTESIAN_POINT ( 'NONE',  ( -54.57824257350981156, -24.66019654487199375, 8.947790411086119278 ) ) ;
#87623=CARTESIAN_POINT ( 'NONE',  ( 3.385237411341575964, -20.22741857368478335, 11.49999999999998934 ) ) ;
#87625=ORIENTED_EDGE ( 'NONE', *, *, #25739, .F. ) ;
#87629=CARTESIAN_POINT ( 'NONE',  ( 18.33865528945960577, 14.04639130150205872, -1.500000000000002220 ) ) ;
#87630=CARTESIAN_POINT ( 'NONE',  ( -104.5103158840345117, -24.66019654487200441, 8.947790411086108620 ) ) ;
#87631=CARTESIAN_POINT ( 'NONE',  ( -5.548086588741434788, -19.59138962566686004, -1.500000000000002220 ) ) ;
#87632=VERTEX_POINT ( 'NONE', #89632 ) ;
#87636=CARTESIAN_POINT ( 'NONE',  ( -112.9228709571500531, -23.47593901973090524, -1.443836447538996648 ) ) ;
#87637=CARTESIAN_POINT ( 'NONE',  ( -63.52287095715010423, -23.95044443724991723, 10.65354141964649948 ) ) ;
#87638=VERTEX_POINT ( 'NONE', #27240 ) ;
#87639=CARTESIAN_POINT ( 'NONE',  ( -29.24636659181000198, -24.76881433503877616, 4.940287988257682450 ) ) ;
#87641=VERTEX_POINT ( 'NONE', #11502 ) ;
#87642=CARTESIAN_POINT ( 'NONE',  ( -3.546427018491999483, -20.45703643143680850, 11.49999999999998934 ) ) ;
#87644=EDGE_CURVE ( 'NONE', #62185, #92377, #41464, .T. ) ;
#87645=ORIENTED_EDGE ( 'NONE', *, *, #17753, .F. ) ;
#87646=CARTESIAN_POINT ( 'NONE',  ( -125.5192795453270378, -25.00158670708911046, 2.256160236439218369 ) ) ;
#87649=B_SPLINE_CURVE_WITH_KNOTS ( 'NONE', 3,
 ( #19262, #26886, #4560, #50233, #66482, #35508 ),
 .UNSPECIFIED., .F., .F.,
 ( 4, 2, 4 ),
 ( 1.570755371633856203E-05, 0.001396183895866085368, 0.002776660238015832109 ),
 .UNSPECIFIED. ) ;
#87650=CARTESIAN_POINT ( 'NONE',  ( -122.6228709571500417, -24.66019654487199730, 8.947790411086121054 ) ) ;
#87651=ORIENTED_EDGE ( 'NONE', *, *, #55997, .T. ) ;
#87652=ORIENTED_EDGE ( 'NONE', *, *, #12814, .T. ) ;
#87654=CARTESIAN_POINT ( 'NONE',  ( -98.52287095715006160, -23.48786465467241769, 11.44779295918254114 ) ) ;
#87655=CARTESIAN_POINT ( 'NONE',  ( -30.93930388503498818, -23.47593901973090169, -1.443836447538998424 ) ) ;
#87656=CARTESIAN_POINT ( 'NONE',  ( 9.306852550357104903, -20.00191182576189064, 11.49999999999999645 ) ) ;
#87657=ORIENTED_EDGE ( 'NONE', *, *, #26200, .F. ) ;
#87658=CARTESIAN_POINT ( 'NONE',  ( -47.62287095715004881, -23.73934037231756733, 11.05740245334329153 ) ) ;
#87659=CARTESIAN_POINT ( 'NONE',  ( 18.14931799402153345, 13.46472642042223633, -1.500000000000002220 ) ) ;
#87660=CARTESIAN_POINT ( 'NONE',  ( -79.11611000704996854, -25.13069340115296058, 2.947789388436138580 ) ) ;
#87663=ORIENTED_EDGE ( 'NONE', *, *, #94435, .F. ) ;
#87665=CARTESIAN_POINT ( 'NONE',  ( -84.62287095715005592, -29.50248528299804818, 1.056150453629038477 ) ) ;
#87666=CARTESIAN_POINT ( 'NONE',  ( -57.54249901568284997, -24.35071581493543036, 9.817618358456028815 ) ) ;
#87668=CARTESIAN_POINT ( 'NONE',  ( -0.1268723920767304558, 21.18662008908366445, -1.500000000000002220 ) ) ;
#87669=CARTESIAN_POINT ( 'NONE',  ( -34.62287095715005592, -23.96177878511307568, 10.65340807706330573 ) ) ;
#87671=CARTESIAN_POINT ( 'NONE',  ( -32.52287095715006160, -23.47596703998600631, 11.44779298504229459 ) ) ;
#87672=CARTESIAN_POINT ( 'NONE',  ( -82.52287095715006160, -29.50250243563736774, 8.947779886222141599 ) ) ;
#87673=CARTESIAN_POINT ( 'NONE',  ( -4.330935931041660858, -21.79039167146679290, -1.500000000000002220 ) ) ;
#87674=CARTESIAN_POINT ( 'NONE',  ( -114.5149094425525504, -24.65952944569305316, 1.056160979905706121 ) ) ;
#87675=ORIENTED_EDGE ( 'NONE', *, *, #57419, .T. ) ;
#87678=CARTESIAN_POINT ( 'NONE',  ( -19.24332624019526961, -2.196797614219411443, 11.49999999999999645 ) ) ;
#87679=PLANE ( 'NONE',  #59293 ) ;
#87680=CARTESIAN_POINT ( 'NONE',  ( -44.92287095715005307, -23.47596703998600631, 11.44779298504227683 ) ) ;
#87681=B_SPLINE_CURVE_WITH_KNOTS ( 'NONE', 3,
 ( #83536, #22127, #83032, #59218, #51107, #5919 ),
 .UNSPECIFIED., .F., .F.,
 ( 4, 2, 4 ),
 ( 6.391158118967745954E-06, 0.001387004593080787230, 0.002767618028042606766 ),
 .UNSPECIFIED. ) ;
#87682=CARTESIAN_POINT ( 'NONE',  ( 12.63578256557813795, 14.83599306707809085, 11.49999999999998934 ) ) ;
#87683=CARTESIAN_POINT ( 'NONE',  ( 17.72605931280000391, -11.99821887194124770, -1.500000000000002220 ) ) ;
#87684=DIRECTION ( 'NONE',  ( 1.000000000000000000, 3.773278334444166432E-23, 8.201307841325785021E-29 ) ) ;
#87685=CARTESIAN_POINT ( 'NONE',  ( -60.66488840562722373, -23.48786465467241058, 11.44779295918254824 ) ) ;
#87687=CARTESIAN_POINT ( 'NONE',  ( -120.5895376238167245, -24.99156044556202971, 7.747789690856173195 ) ) ;
#87688=CARTESIAN_POINT ( 'NONE',  ( 19.62911079104473444, -11.51699945595908758, -1.500000000000002220 ) ) ;
#87689=ADVANCED_FACE ( 'NONE', ( #58195 ), #67168, .T. ) ;
#87691=CARTESIAN_POINT ( 'NONE',  ( -102.5574996872169891, -23.73766607897671577, -1.055555164236430254 ) ) ;
#87692=DIRECTION ( 'NONE',  ( -3.773278334453080206E-23, 0.9999999999976377785, 2.173523156925979975E-06 ) ) ;
#87693=CARTESIAN_POINT ( 'NONE',  ( -17.57349146297605103, 9.389787994052484876, 11.49999999999999645 ) ) ;
#87694=CARTESIAN_POINT ( 'NONE',  ( -69.52287095715007581, -24.51283580621366198, 0.6167428607019654896 ) ) ;
#87695=ADVANCED_FACE ( 'NONE', ( #18122 ), #49088, .F. ) ;
#87696=CARTESIAN_POINT ( 'NONE',  ( -98.89303308397303738, -29.50249626970221328, 6.110940943921145951 ) ) ;
#87702=CARTESIAN_POINT ( 'NONE',  ( -15.83346750871019992, -14.79491179806518630, -1.500000000000002220 ) ) ;
#87703=PLANE ( 'NONE',  #25296 ) ;
#87704=CARTESIAN_POINT ( 'NONE',  ( 15.68791110202092476, 11.56419973807686219, -1.500000000000002220 ) ) ;
#87705=ADVANCED_FACE ( 'NONE', ( #37351 ), #59694, .T. ) ;
#87706=CARTESIAN_POINT ( 'NONE',  ( -55.52200627751408746, -23.48786465467241413, 11.44779295918254647 ) ) ;
#87708=DIRECTION ( 'NONE',  ( 1.000000000000000000, 3.773278334444167608E-23, 8.201307833595939069E-29 ) ) ;
#87709=CARTESIAN_POINT ( 'NONE',  ( -9.871001836803966256, -17.81128643866572148, 11.49999999999999645 ) ) ;
#87710=CARTESIAN_POINT ( 'NONE',  ( -42.62287095715004881, -29.50248528299804818, 1.056150453629031594 ) ) ;
#87711=EDGE_CURVE ( 'NONE', #20125, #13115, #95771, .T. ) ;
#87715=B_SPLINE_CURVE_WITH_KNOTS ( 'NONE', 3,
 ( #17733, #80128, #25339, #63429 ),
 .UNSPECIFIED., .F., .F.,
 ( 4, 4 ),
 ( 0.000000000000000000, 9.999999999998897304E-05 ),
 .UNSPECIFIED. ) ;
#87717=CARTESIAN_POINT ( 'NONE',  ( -72.52287095715003318, -23.73907113216989373, -1.053371485793251905 ) ) ;
#87718=CARTESIAN_POINT ( 'NONE',  ( -122.6228709571500417, -29.50250786944525672, 11.44777988621622811 ) ) ;
#87719=CARTESIAN_POINT ( 'NONE',  ( -39.10567952407142656, -25.31628543545969379, 4.652296572693673582 ) ) ;
#87721=CARTESIAN_POINT ( 'NONE',  ( -126.6228709571500559, -29.50250243563736774, 8.947779886222132717 ) ) ;
#87722=B_SPLINE_CURVE_WITH_KNOTS ( 'NONE', 3,
 ( #6470, #76459, #44536, #37917 ),
 .UNSPECIFIED., .F., .F.,
 ( 4, 4 ),
 ( 0.000000000000000000, 2.030847249360049860E-05 ),
 .UNSPECIFIED. ) ;
#87723=CARTESIAN_POINT ( 'NONE',  ( -55.92287095715006018, -23.47593901973090169, -1.443836447538997758 ) ) ;
#87725=CARTESIAN_POINT ( 'NONE',  ( -66.55385742457673359, -23.96169478059713143, 10.65365249895718058 ) ) ;
#87726=AXIS2_PLACEMENT_3D ( 'NONE', #49272, #95422, #88316 ) ;
#87727=CARTESIAN_POINT ( 'NONE',  ( 12.10309942457327992, -19.51426552955538085, 11.49999999999999645 ) ) ;
#87728=CARTESIAN_POINT ( 'NONE',  ( 21.73672277138745201, -6.736064506363727666, 11.49999999999998934 ) ) ;
#87729=FACE_OUTER_BOUND ( 'NONE', #85966, .T. ) ;
#87730=CARTESIAN_POINT ( 'NONE',  ( -74.62287095715005592, -29.50250786944525672, 11.44777988621623699 ) ) ;
#87731=CARTESIAN_POINT ( 'NONE',  ( -90.51647974171660849, -23.85016227208580730, -0.8807180028928305315 ) ) ;
#87734=CARTESIAN_POINT ( 'NONE',  ( -13.92312151449838531, -16.86485062357919773, -1.500000000000002220 ) ) ;
#87736=CARTESIAN_POINT ( 'NONE',  ( -115.6228709571500275, -24.52232992886362695, 0.6492154411906169154 ) ) ;
#87737=FACE_OUTER_BOUND ( 'NONE', #19509, .T. ) ;
#87739=VERTEX_POINT ( 'NONE', #83000 ) ;
#87740=CARTESIAN_POINT ( 'NONE',  ( -12.12210191164509965, 16.44476101713275185, -1.500000000000002220 ) ) ;
#87741=ORIENTED_EDGE ( 'NONE', *, *, #37414, .F. ) ;
#87743=B_SPLINE_CURVE_WITH_KNOTS ( 'NONE', 3,
 ( #71773, #72277, #80379, #64685 ),
 .UNSPECIFIED., .F., .F.,
 ( 4, 4 ),
 ( 6.938893903907227607E-18, 9.999999999999593903E-05 ),
 .UNSPECIFIED. ) ;
#87744=CARTESIAN_POINT ( 'NONE',  ( 22.64363655503811046, -4.068770074275382953, -1.500000000000002220 ) ) ;
#87746=EDGE_LOOP ( 'NONE', ( #24999, #62196, #93852, #75946 ) ) ;
#87747=CARTESIAN_POINT ( 'NONE',  ( -114.5228709571500616, -23.48786465467241769, 11.44779295918253936 ) ) ;
#87749=B_SPLINE_CURVE_WITH_KNOTS ( 'NONE', 3,
 ( #44512, #53133, #100258, #6939, #7431, #90678 ),
 .UNSPECIFIED., .F., .F.,
 ( 4, 2, 4 ),
 ( 6.384118694664676754E-06, 0.001386860460836404803, 0.002767336802978144928 ),
 .UNSPECIFIED. ) ;
#87751=CARTESIAN_POINT ( 'NONE',  ( -53.57809142228946087, -24.66019654487199375, 8.947790411086122830 ) ) ;
#87752=CARTESIAN_POINT ( 'NONE',  ( 18.99370601119529312, 9.851043883551550806, 11.49999999999999645 ) ) ;
#87754=ORIENTED_EDGE ( 'NONE', *, *, #36844, .F. ) ;
#87755=CARTESIAN_POINT ( 'NONE',  ( -4.073883676365832152, 21.86232641878667593, -1.500000000000002220 ) ) ;
#87756=CARTESIAN_POINT ( 'NONE',  ( -20.26430336558559020, 4.098603726722801710, -1.500000000000002220 ) ) ;
#87757=EDGE_CURVE ( 'NONE', #17644, #65087, #82464, .T. ) ;
#87763=ORIENTED_EDGE ( 'NONE', *, *, #14792, .T. ) ;
#87764=CARTESIAN_POINT ( 'NONE',  ( -55.52287095715006870, -23.47596703998600631, 11.44779298504228926 ) ) ;
#87765=ORIENTED_EDGE ( 'NONE', *, *, #21830, .F. ) ;
#87767=CARTESIAN_POINT ( 'NONE',  ( -70.44747929723452273, -25.12380530056864103, 7.096986476995511772 ) ) ;
#87768=CARTESIAN_POINT ( 'NONE',  ( 10.02768300834196502, -18.34552750054021786, -1.500000000000002220 ) ) ;
#87769=CARTESIAN_POINT ( 'NONE',  ( -6.606886629844116676, -20.84447163495035937, 11.49999999999999645 ) ) ;
#87770=CARTESIAN_POINT ( 'NONE',  ( -26.33488822642538452, -24.89279768858262187, 6.524121853396118276 ) ) ;
#87771=PLANE ( 'NONE',  #79108 ) ;
#87772=CARTESIAN_POINT ( 'NONE',  ( 9.993301969596378953, 20.15287186522775542, -1.500000000000002220 ) ) ;
#87773=CARTESIAN_POINT ( 'NONE',  ( 16.15719879640481338, -13.26386290209467944, 11.49999999999998934 ) ) ;
#87774=CARTESIAN_POINT ( 'NONE',  ( -26.12923826827997686, -24.88148856164281852, 5.595194550550813162 ) ) ;
#87775=CARTESIAN_POINT ( 'NONE',  ( -53.55620429048340725, -24.64898659630527789, 1.056161002820820594 ) ) ;
#87779=EDGE_LOOP ( 'NONE', ( #65883, #54700, #49654, #36059 ) ) ;
#87780=VECTOR ( 'NONE', #93801, 1000.000000000000114 ) ;
#87782=EDGE_LOOP ( 'NONE', ( #21279, #99086, #46754, #7125 ) ) ;
#87783=CARTESIAN_POINT ( 'NONE',  ( -20.78045986758521835, -5.208592277829342088, -1.500000000000002220 ) ) ;
#87784=B_SPLINE_CURVE_WITH_KNOTS ( 'NONE', 3,
 ( #95431, #3103, #34038, #65014 ),
 .UNSPECIFIED., .F., .F.,
 ( 4, 4 ),
 ( 0.000000000000000000, 9.999999999998897304E-05 ),
 .UNSPECIFIED. ) ;
#87785=CARTESIAN_POINT ( 'NONE',  ( 3.152853332073482839, 22.16862046936333286, 11.49999999999999645 ) ) ;
#87788=CARTESIAN_POINT ( 'NONE',  ( 1.225302832070333636, 21.05158420706169764, 11.49999999999998934 ) ) ;
#87789=CARTESIAN_POINT ( 'NONE',  ( -30.60817598444602794, -24.49002127936269702, 9.440108529385042857 ) ) ;
#87790=CARTESIAN_POINT ( 'NONE',  ( 17.47191945374660094, 9.613082372698542599, -1.500000000000002220 ) ) ;
#87792=CARTESIAN_POINT ( 'NONE',  ( -46.62287095715004881, -29.50250243563736774, 8.947779886222146928 ) ) ;
#87793=CARTESIAN_POINT ( 'NONE',  ( -21.92701646642465008, -2.088449908657787457, -1.500000000000002220 ) ) ;
#87794=ORIENTED_EDGE ( 'NONE', *, *, #68567, .T. ) ;
#87795=CARTESIAN_POINT ( 'NONE',  ( -116.5892976607136262, -24.34968618360935366, 0.1864209137779019310 ) ) ;
#87796=LINE ( 'NONE', #58357, #17322 ) ;
#87797=CARTESIAN_POINT ( 'NONE',  ( -41.36802863981588274, -25.31624677975437976, 5.250400717901936076 ) ) ;
#87798=CARTESIAN_POINT ( 'NONE',  ( -29.83743700494218842, -25.25831489976056687, 4.936952632524851836 ) ) ;
#87800=FACE_OUTER_BOUND ( 'NONE', #42736, .T. ) ;
#87803=CARTESIAN_POINT ( 'NONE',  ( -18.01091527469349529, -11.40912366963296698, 11.49999999999998934 ) ) ;
#87804=CARTESIAN_POINT ( 'NONE',  ( -70.74026866089610621, -25.31511106678998502, 4.894904372220056921 ) ) ;
#87806=FACE_OUTER_BOUND ( 'NONE', #83730, .T. ) ;
#87808=CARTESIAN_POINT ( 'NONE',  ( 21.71239400539012721, -6.292901409244172406, -1.500000000000002220 ) ) ;
#87811=CARTESIAN_POINT ( 'NONE',  ( -50.92779201898847674, -25.31191645034120441, 5.304553393514395587 ) ) ;
#87812=CARTESIAN_POINT ( 'NONE',  ( -120.5562042904833930, -23.47596703998600631, 11.44779298504227683 ) ) ;
#87813=CARTESIAN_POINT ( 'NONE',  ( 17.05426814964238957, 9.943002105365778220, 11.49999999999999645 ) ) ;
#87819=CARTESIAN_POINT ( 'NONE',  ( -127.4728709594060092, -25.40676174399604648, 8.000950335807015534 ) ) ;
#87820=ADVANCED_FACE ( 'NONE', ( #5392 ), #44464, .F. ) ;
#87821=CARTESIAN_POINT ( 'NONE',  ( -124.5548821316224064, -24.35071581493544457, 9.817618358456016381 ) ) ;
#87822=CARTESIAN_POINT ( 'NONE',  ( -76.55620429048342146, -24.64898659630528854, 1.056161002820828587 ) ) ;
#87824=EDGE_CURVE ( 'NONE', #8909, #35157, #18202, .T. ) ;
#87825=PLANE ( 'NONE',  #51296 ) ;
#87826=CARTESIAN_POINT ( 'NONE',  ( 2.545096341412688812, 19.61957628810408849, 11.49999999999998934 ) ) ;
#87827=VERTEX_POINT ( 'NONE', #68292 ) ;
#87829=B_SPLINE_CURVE_WITH_KNOTS ( 'NONE', 3,
 ( #35196, #19454, #65666, #27585, #19952, #20447, #81862, #49433, #80366, #26585, #27081, #88485, #66168, #11355, #58047, #50420 ),
 .UNSPECIFIED., .F., .F.,
 ( 4, 2, 2, 2, 2, 2, 2, 4 ),
 ( 0.000000000000000000, 0.0002052712941191513771, 0.0004105425882383027542, 0.0008210851764766055084, 0.001026356470595756777, 0.001231627764714908263, 0.001436899058834059748, 0.001642170352953211017 ),
 .UNSPECIFIED. ) ;
#87830=CARTESIAN_POINT ( 'NONE',  ( 2.532258636284850706, -20.04889675553949147, 11.49999999999999645 ) ) ;
#87834=VERTEX_POINT ( 'NONE', #45467 ) ;
#87837=CARTESIAN_POINT ( 'NONE',  ( -88.88918693012686845, -25.26680044519436663, 6.101892079195562424 ) ) ;
#87839=CARTESIAN_POINT ( 'NONE',  ( -62.55620429048337883, -23.48786465467241413, 11.44779295918254824 ) ) ;
#87840=CARTESIAN_POINT ( 'NONE',  ( -86.62287095715005592, -24.66019654487199375, 8.947790411086124607 ) ) ;
#87841=CARTESIAN_POINT ( 'NONE',  ( 12.85705330080557829, 15.37097598829428513, 11.49999999999998934 ) ) ;
#87843=CARTESIAN_POINT ( 'NONE',  ( -67.58953762381672448, -23.48783264082478794, -1.443836473390067265 ) ) ;
#87845=CARTESIAN_POINT ( 'NONE',  ( -73.62287095715007013, -23.47596703998600276, 11.44779298504227860 ) ) ;
#87846=CARTESIAN_POINT ( 'NONE',  ( -33.62287095715007013, -24.34917612406836795, 0.1852690917426547956 ) ) ;
#87850=CARTESIAN_POINT ( 'NONE',  ( -73.63478338152101799, -24.15543982623907127, -0.2315651400026654816 ) ) ;
#87851=CARTESIAN_POINT ( 'NONE',  ( -45.58953762381671737, -23.47596703998600276, 11.44779298504227505 ) ) ;
#87852=CARTESIAN_POINT ( 'NONE',  ( -100.9371098987261917, -25.30060005375480614, 6.009289253917324380 ) ) ;
#87853=ORIENTED_EDGE ( 'NONE', *, *, #37536, .T. ) ;
#87854=CARTESIAN_POINT ( 'NONE',  ( -20.07547297788957152, 3.163885811906596679, 11.49999999999998934 ) ) ;
#87856=CARTESIAN_POINT ( 'NONE',  ( -32.55273188169832110, -23.96119346886880663, -0.6495511937831992544 ) ) ;
#87857=CARTESIAN_POINT ( 'NONE',  ( -127.5906370802701844, -23.48786465467242124, 11.44779295918253403 ) ) ;
#87859=CARTESIAN_POINT ( 'NONE',  ( -59.60446161964285494, -23.73791477778911840, 11.05961554403171299 ) ) ;
#87864=CARTESIAN_POINT ( 'NONE',  ( 14.81885032312887240, -15.09863332352077592, 11.49999999999999645 ) ) ;
#87866=CARTESIAN_POINT ( 'NONE',  ( 19.88262469969689050, -9.776007750257504014, 11.49999999999998934 ) ) ;
#87868=CARTESIAN_POINT ( 'NONE',  ( 16.43461662053371697, -12.34185696772103391, -1.500000000000002220 ) ) ;
#87870=CARTESIAN_POINT ( 'NONE',  ( -113.5562042904833930, -23.47596703998600631, 11.44779298504227683 ) ) ;
#87871=ORIENTED_EDGE ( 'NONE', *, *, #84386, .F. ) ;
#87874=ORIENTED_EDGE ( 'NONE', *, *, #55166, .F. ) ;
#87876=ORIENTED_EDGE ( 'NONE', *, *, #41886, .F. ) ;
#87878=B_SPLINE_CURVE_WITH_KNOTS ( 'NONE', 3,
 ( #88738, #87224, #26827, #3504, #19205, #17720 ),
 .UNSPECIFIED., .F., .F.,
 ( 4, 2, 4 ),
 ( 0.000000000000000000, 0.001380764517854763448, 0.002761529035709526896 ),
 .UNSPECIFIED. ) ;
#87881=CARTESIAN_POINT ( 'NONE',  ( 12.06641648444584369, 16.80774221200798735, -1.500000000000002220 ) ) ;
#87882=CARTESIAN_POINT ( 'NONE',  ( 21.13687465659472409, 4.681744431724916389, 11.49999999999999645 ) ) ;
#87886=CARTESIAN_POINT ( 'NONE',  ( -8.193370562272118462, -20.86776251599019361, -1.500000000000002220 ) ) ;
#87887=CARTESIAN_POINT ( 'NONE',  ( -124.5895376238167245, -23.48783264082479505, -1.443836473390058828 ) ) ;
#87888=CARTESIAN_POINT ( 'NONE',  ( -102.5228709571501042, -24.66019654487200441, 8.947790411086119278 ) ) ;
#87890=DIRECTION ( 'NONE',  ( -3.773278334453079618E-23, 0.9999999999976377785, 2.173523156925979975E-06 ) ) ;
#87891=CARTESIAN_POINT ( 'NONE',  ( -116.4728709548940628, -25.21112548385455554, 2.000950967214103038 ) ) ;
#87892=B_SPLINE_SURFACE_WITH_KNOTS ( 'NONE', 3, 3, ( 
 ( #965, #93810, #24793, #77571 ),
 ( #92802, #30910, #71490, #7576 ),
 ( #86201, #63896, #23283, #8075 ),
 ( #78567, #458, #40029, #70988 ),
 ( #94304, #62371, #1477, #39022 ),
 ( #32417, #17184, #15685, #38524 ),
 ( #69479, #31414, #93300, #19178 ),
 ( #73977, #73478, #4475, #26305 ),
 ( #57765, #50638, #35424, #10076 ),
 ( #43035, #27796, #19673, #87706 ) ),
 .UNSPECIFIED., .F., .F., .F.,
 ( 4, 3, 3, 4 ),
 ( 4, 4 ),
 ( 0.7022005934544806038, 0.7765311282028795059, 0.8508616629512784080, 0.9995227324480763231 ),
 ( 0.7495844612969405629, 0.7510439278013898434 ),
 .UNSPECIFIED. ) ;
#87895=CARTESIAN_POINT ( 'NONE',  ( -46.62370101417344870, -24.66019654487199375, 8.947790411086122830 ) ) ;
#87897=EDGE_LOOP ( 'NONE', ( #50316, #22550, #58813, #76983 ) ) ;
#87898=B_SPLINE_CURVE_WITH_KNOTS ( 'NONE', 3,
 ( #4544, #72553, #17759, #57837 ),
 .UNSPECIFIED., .F., .F.,
 ( 4, 4 ),
 ( 2.226473276209221022E-11, 0.003119410830149253137 ),
 .UNSPECIFIED. ) ;
#87901=CARTESIAN_POINT ( 'NONE',  ( -19.34623641613454836, -8.721557147202650739, -1.500000000000002220 ) ) ;
#87902=ORIENTED_EDGE ( 'NONE', *, *, #83463, .T. ) ;
#87903=CARTESIAN_POINT ( 'NONE',  ( -88.63862431805245023, -23.73766607897670511, -1.055555164236456678 ) ) ;
#87905=CARTESIAN_POINT ( 'NONE',  ( 16.38291735060997567, -14.39268585342195905, 11.49999999999998934 ) ) ;
#87906=CARTESIAN_POINT ( 'NONE',  ( -103.5098569560838371, -24.66019654487200086, 8.947790411086115725 ) ) ;
#87908=CARTESIAN_POINT ( 'NONE',  ( -35.62287095715004170, -24.14321612903113845, -0.2833117244521695666 ) ) ;
#87909=CARTESIAN_POINT ( 'NONE',  ( -6.606886629844116676, -20.84447163495035937, -1.500000000000002220 ) ) ;
#87911=EDGE_LOOP ( 'NONE', ( #90269, #64566, #37693, #73317 ) ) ;
#87915=CARTESIAN_POINT ( 'NONE',  ( -30.57842286860461911, -25.26764614148072496, 6.117730354831462769 ) ) ;
#87916=EDGE_LOOP ( 'NONE', ( #31351, #81777, #23321, #48185 ) ) ;
#87917=AXIS2_PLACEMENT_3D ( 'NONE', #35048, #27925, #78813 ) ;
#87918=DIRECTION ( 'NONE',  ( -3.773278334453079030E-23, 0.9999999999976377785, 2.173523156925979128E-06 ) ) ;
#87919=CARTESIAN_POINT ( 'NONE',  ( -82.64079165572177033, -23.73766607897671221, -1.055555164236435362 ) ) ;
#87920=B_SPLINE_CURVE_WITH_KNOTS ( 'NONE', 3,
 ( #90104, #20578, #52043, #51051 ),
 .UNSPECIFIED., .F., .F.,
 ( 4, 4 ),
 ( 0.000000000000000000, 9.999999999997510880E-05 ),
 .UNSPECIFIED. ) ;
#87921=CARTESIAN_POINT ( 'NONE',  ( -19.98547761299008130, 7.154247560337752887, 11.49999999999998934 ) ) ;
#87923=CARTESIAN_POINT ( 'NONE',  ( -130.5728709571500588, -24.37728322581796192, 9.960208392924581489 ) ) ;
#87924=CARTESIAN_POINT ( 'NONE',  ( -92.62287095715005592, -24.64965695001469115, 8.947790433994180503 ) ) ;
#87925=FACE_OUTER_BOUND ( 'NONE', #34601, .T. ) ;
#87926=CARTESIAN_POINT ( 'NONE',  ( -11.04204518803028456, 15.98388583709530941, 11.49999999999998934 ) ) ;
#87927=CARTESIAN_POINT ( 'NONE',  ( -45.64360056886428652, -24.40034930558990922, 0.3402023900116019073 ) ) ;
#87929=CARTESIAN_POINT ( 'NONE',  ( 1.133552453683672745, -19.47370032599940615, 11.49999999999999645 ) ) ;
#87933=EDGE_LOOP ( 'NONE', ( #49241, #45883, #23088 ) ) ;
#87936=CARTESIAN_POINT ( 'NONE',  ( -90.52287095715009002, -23.48783264082477373, -1.443836473390088582 ) ) ;
#87937=AXIS2_PLACEMENT_3D ( 'NONE', #43149, #27911, #89810 ) ;
#87938=CARTESIAN_POINT ( 'NONE',  ( -81.67724764284677974, -25.24813850574973628, 6.915643883124781510 ) ) ;
#87939=CARTESIAN_POINT ( 'NONE',  ( 0.7877182283408599162, 19.66719298131377514, 11.49999999999998934 ) ) ;
#87942=EDGE_CURVE ( 'NONE', #45475, #23903, #8381, .T. ) ;
#87944=DIRECTION ( 'NONE',  ( 0.000000000000000000, -2.173523156925979552E-06, 0.9999999999976378895 ) ) ;
#87948=ORIENTED_EDGE ( 'NONE', *, *, #83123, .T. ) ;
#87949=CARTESIAN_POINT ( 'NONE',  ( -125.5228709571501184, -23.85229601348998330, 10.88205029486207920 ) ) ;
#87951=CARTESIAN_POINT ( 'NONE',  ( -108.9960569403308313, -25.24778904441513916, 3.815199558290551796 ) ) ;
#87952=CARTESIAN_POINT ( 'NONE',  ( -29.52287095715006515, -24.41935721893828415, 9.387660007492499403 ) ) ;
#87953=DIRECTION ( 'NONE',  ( -3.773278334453080206E-23, 0.9999999999976377785, 2.173523156925979975E-06 ) ) ;
#87954=CARTESIAN_POINT ( 'NONE',  ( -69.41551097411255000, -25.31201709968604874, 5.862899404653265201 ) ) ;
#87956=CARTESIAN_POINT ( 'NONE',  ( -79.52287095715006160, -23.96127896941631974, -0.6493128931038034679 ) ) ;
#87957=CARTESIAN_POINT ( 'NONE',  ( -14.97016004668225264, 13.15154794113874637, 11.49999999999998934 ) ) ;
#87959=CARTESIAN_POINT ( 'NONE',  ( -75.65600689415964553, -23.48786465467241058, 11.44779295918254824 ) ) ;
#87960=CARTESIAN_POINT ( 'NONE',  ( 11.24879072547334324, 16.40116332625411033, -1.500000000000002220 ) ) ;
#87961=VERTEX_POINT ( 'NONE', #15981 ) ;
#87963=CARTESIAN_POINT ( 'NONE',  ( -125.5228709571500616, -24.82558206586144678, 1.605769216559449042 ) ) ;
#87964=CARTESIAN_POINT ( 'NONE',  ( -117.6228709571500559, -23.72773821059535493, 11.05748984161097503 ) ) ;
#87965=CARTESIAN_POINT ( 'NONE',  ( -80.62512084407954660, -24.92592662359561473, 8.075495903017996469 ) ) ;
#87966=CARTESIAN_POINT ( 'NONE',  ( 11.01739540223112357, 17.63107602209319680, 11.49999999999999645 ) ) ;
#87967=DIRECTION ( 'NONE',  ( -3.773278334453079030E-23, 0.9999999999976377785, 2.173523156925979128E-06 ) ) ;
#87968=CARTESIAN_POINT ( 'NONE',  ( -59.62287095715004881, -23.47593901973091235, -1.443836447539007972 ) ) ;
#87969=CARTESIAN_POINT ( 'NONE',  ( 13.94817355369617751, 18.09530419158152625, 11.49999999999999645 ) ) ;
#87971=ORIENTED_EDGE ( 'NONE', *, *, #77646, .T. ) ;
#87972=B_SPLINE_SURFACE_WITH_KNOTS ( 'NONE', 3, 1, ( 
 ( #45556, #21687 ),
 ( #53170, #67394 ),
 ( #76476, #83593 ),
 ( #90721, #75977 ),
 ( #30309, #59274 ),
 ( #6486, #74979 ),
 ( #98317, #21194 ) ),
 .UNSPECIFIED., .F., .F., .F.,
 ( 4, 1, 1, 1, 4 ),
 ( 2, 2 ),
 ( 0.000000000000000000, 0.2538796003266583501, 0.5030089172783559492, 0.7502910806899644180, 1.000000000000000000 ),
 ( 0.000000000000000000, 1.000000000000000000 ),
 .UNSPECIFIED. ) ;
#87973=CARTESIAN_POINT ( 'NONE',  ( -54.92287095715008860, -23.47593901973090880, -1.443836447538998202 ) ) ;
#87974=CARTESIAN_POINT ( 'NONE',  ( -127.6245366232018057, -23.73766607897670511, -1.055555164236447130 ) ) ;
#87975=ORIENTED_EDGE ( 'NONE', *, *, #86241, .F. ) ;
#87976=CARTESIAN_POINT ( 'NONE',  ( -13.29518446780263119, -15.22762515321373478, 11.49999999999998934 ) ) ;
#87977=EDGE_CURVE ( 'NONE', #11670, #76617, #22585, .T. ) ;
#87978=CARTESIAN_POINT ( 'NONE',  ( -106.5228709571500758, -24.66019654487200441, 8.947790411086112172 ) ) ;
#87983=CARTESIAN_POINT ( 'NONE',  ( -97.62287095715005592, -23.48783264082478794, -1.443836473390061936 ) ) ;
#87984=CARTESIAN_POINT ( 'NONE',  ( -104.6228709571500559, -23.47596703998600631, 11.44779298504227860 ) ) ;
#87985=CARTESIAN_POINT ( 'NONE',  ( 6.038693664686949347, 19.05185810397003721, -1.500000000000002220 ) ) ;
#87987=CARTESIAN_POINT ( 'NONE',  ( 2.438461900574103502, 20.79476225230834174, 11.49999999999999645 ) ) ;
#87988=CARTESIAN_POINT ( 'NONE',  ( -29.80787223232210437, -25.25360408432739945, 5.314274568547425304 ) ) ;
#87990=CARTESIAN_POINT ( 'NONE',  ( 13.62230711432095553, -17.35066874027886286, 11.49999999999998934 ) ) ;
#87991=CARTESIAN_POINT ( 'NONE',  ( -39.85544541354917669, -25.31589298330722571, 4.937102986595060194 ) ) ;
#87994=FACE_OUTER_BOUND ( 'NONE', #88026, .T. ) ;
#87995=CARTESIAN_POINT ( 'NONE',  ( -37.62287095715005592, -29.50248528299804818, 1.056150453629031594 ) ) ;
#87996=PLANE ( 'NONE',  #49461 ) ;
#87997=ORIENTED_EDGE ( 'NONE', *, *, #73131, .F. ) ;
#87998=DIRECTION ( 'NONE',  ( 0.000000000000000000, 0.9999999999976377785, 2.173523156925979975E-06 ) ) ;
#87999=VERTEX_POINT ( 'NONE', #70290 ) ;
#88003=CARTESIAN_POINT ( 'NONE',  ( -51.52287095715006160, -24.50216790748204687, 0.6166512839542488411 ) ) ;
#88004=CARTESIAN_POINT ( 'NONE',  ( 7.506095096478735407, 19.11734572241606145, -1.500000000000002220 ) ) ;
#88005=VERTEX_POINT ( 'NONE', #77876 ) ;
#88008=CARTESIAN_POINT ( 'NONE',  ( -83.52287095715000476, -24.34917612406836795, 0.1852690917426532413 ) ) ;
#88009=CARTESIAN_POINT ( 'NONE',  ( -15.13915969582853549, -16.40262476207453801, 11.49999999999998934 ) ) ;
#88015=CARTESIAN_POINT ( 'NONE',  ( -65.52287095715006160, -24.99132157543083821, 2.256160258750667502 ) ) ;
#88017=CARTESIAN_POINT ( 'NONE',  ( 19.25983760003161294, 7.974354923662064998, 11.49999999999998934 ) ) ;
#88019=PLANE ( 'NONE',  #24708 ) ;
#88020=VERTEX_POINT ( 'NONE', #32715 ) ;
#88022=ORIENTED_EDGE ( 'NONE', *, *, #7505, .F. ) ;
#88023=VECTOR ( 'NONE', #96657, 1000.000000000000114 ) ;
#88024=DIRECTION ( 'NONE',  ( -3.773278334453079618E-23, 0.9999999999976377785, 2.173523156925979975E-06 ) ) ;
#88025=CARTESIAN_POINT ( 'NONE',  ( -17.44821286160079410, -11.81026508430653088, -1.500000000000002220 ) ) ;
#88026=EDGE_LOOP ( 'NONE', ( #35576, #54840, #18808, #53654 ) ) ;
#88032=CARTESIAN_POINT ( 'NONE',  ( -100.7317701684513764, -25.03152445186833219, 7.544846145421804984 ) ) ;
#88033=CARTESIAN_POINT ( 'NONE',  ( -59.61135775242147616, -23.48783264082476308, -1.443836473390097908 ) ) ;
#88034=CARTESIAN_POINT ( 'NONE',  ( 17.51545567653809954, -12.82042131148251229, -1.500000000000002220 ) ) ;
#88035=CARTESIAN_POINT ( 'NONE',  ( -80.60699767246597958, -25.12224391340353691, 7.098406057649814471 ) ) ;
#88036=CARTESIAN_POINT ( 'NONE',  ( -2.790049085472659396, -22.09070898310802633, 11.49999999999999645 ) ) ;
#88042=EDGE_CURVE ( 'NONE', #90447, #41368, #95660, .T. ) ;
#88043=EDGE_CURVE ( 'NONE', #896, #72639, #92609, .T. ) ;
#88047=EDGE_CURVE ( 'NONE', #100004, #79632, #92162, .T. ) ;
#88051=ORIENTED_EDGE ( 'NONE', *, *, #31811, .F. ) ;
#88052=CARTESIAN_POINT ( 'NONE',  ( -130.5728709571500588, -24.30959152078064989, -0.1101050347254430017 ) ) ;
#88053=CARTESIAN_POINT ( 'NONE',  ( -13.11617634606977489, 18.14055439154125438, -1.500000000000002220 ) ) ;
#88054=EDGE_CURVE ( 'NONE', #15484, #62407, #67929, .T. ) ;
#88056=CARTESIAN_POINT ( 'NONE',  ( -112.5526642601108165, -24.35071581493543391, 9.817618358456016381 ) ) ;
#88060=CARTESIAN_POINT ( 'NONE',  ( -125.5228709571500616, -25.00158670708909980, 2.256160236439166411 ) ) ;
#88061=CARTESIAN_POINT ( 'NONE',  ( -63.92296805384962965, -24.66459861931856778, 1.095224832288508976 ) ) ;
#88062=CARTESIAN_POINT ( 'NONE',  ( -4.924063254364682507, -18.92933890202812464, -1.500000000000002220 ) ) ;
#88063=VECTOR ( 'NONE', #61640, 1000.000000000000114 ) ;
#88064=FACE_OUTER_BOUND ( 'NONE', #13721, .T. ) ;
#88065=ORIENTED_EDGE ( 'NONE', *, *, #72726, .F. ) ;
#88066=CARTESIAN_POINT ( 'NONE',  ( -10.19830463584622571, -18.94658877215714909, -1.500000000000002220 ) ) ;
#88068=CARTESIAN_POINT ( 'NONE',  ( -71.08634551208074015, -25.12219073911204248, 6.775733800420372432 ) ) ;
#88071=CARTESIAN_POINT ( 'NONE',  ( -21.95939045666098366, -6.591442671832903777, -1.500000000000002220 ) ) ;
#88073=B_SPLINE_CURVE_WITH_KNOTS ( 'NONE', 3,
 ( #9344, #2253, #17461, #25066, #42328, #80367 ),
 .UNSPECIFIED., .F., .F.,
 ( 4, 2, 4 ),
 ( 1.570755371634052715E-05, 0.001396183895866089705, 0.002776660238015838614 ),
 .UNSPECIFIED. ) ;
#88074=EDGE_CURVE ( 'NONE', #55689, #14852, #9855, .T. ) ;
#88076=CARTESIAN_POINT ( 'NONE',  ( -102.9228709571500673, -23.47596703998600631, 11.44779298504227683 ) ) ;
#88078=CARTESIAN_POINT ( 'NONE',  ( -1.290058840521481454, 20.04182742388497473, 11.49999999999999645 ) ) ;
#88079=CARTESIAN_POINT ( 'NONE',  ( -110.3139465455115129, -25.28814068893017719, 2.832404430835924636 ) ) ;
#88080=CARTESIAN_POINT ( 'NONE',  ( -32.58046570376392026, -24.51419770103159834, 9.386484678747182286 ) ) ;
#88081=CARTESIAN_POINT ( 'NONE',  ( -99.52287095715007581, -24.51283580621461766, 0.6167428607048592859 ) ) ;
#88083=B_SPLINE_CURVE_WITH_KNOTS ( 'NONE', 3,
 ( #28688, #67764, #21060, #98686, #37304, #29180 ),
 .UNSPECIFIED., .F., .F.,
 ( 4, 2, 4 ),
 ( 1.570887131794795405E-05, 0.001396322306279761940, 0.002776935741241575838 ),
 .UNSPECIFIED. ) ;
#88085=CARTESIAN_POINT ( 'NONE',  ( 17.59243620335545799, -9.192777620008959261, -1.500000000000002220 ) ) ;
#88086=EDGE_CURVE ( 'NONE', #64103, #78888, #27903, .T. ) ;
#88087=CARTESIAN_POINT ( 'NONE',  ( -40.52287095715007581, -25.00182538069145011, 7.747789668545104647 ) ) ;
#88088=CARTESIAN_POINT ( 'NONE',  ( -6.756748142665309764, -18.51622224137248907, -1.500000000000002220 ) ) ;
#88089=CARTESIAN_POINT ( 'NONE',  ( -42.65524057351728260, -23.73766607897670156, -1.055555164236442689 ) ) ;
#88091=VECTOR ( 'NONE', #87918, 1000.000000000000114 ) ;
#88092=EDGE_CURVE ( 'NONE', #41774, #24375, #73921, .T. ) ;
#88096=CARTESIAN_POINT ( 'NONE',  ( -111.5228709571500616, -24.51283580621365843, 0.6167428607019709297 ) ) ;
#88097=CARTESIAN_POINT ( 'NONE',  ( -7.709890279958820258, -19.11728055126480186, 11.49999999999999645 ) ) ;
#88098=CARTESIAN_POINT ( 'NONE',  ( -128.5228709571501042, -24.66019654487200441, 8.947790411086108620 ) ) ;
#88100=CARTESIAN_POINT ( 'NONE',  ( 2.978076788109338402, -22.46882643481310282, 11.49999999999999645 ) ) ;
#88102=CARTESIAN_POINT ( 'NONE',  ( -115.5895376238166961, -25.00182538069145721, 7.747789668545099317 ) ) ;
#88103=CARTESIAN_POINT ( 'NONE',  ( -97.63001613934683576, -24.15543982623907837, -0.2315651400026600415 ) ) ;
#88104=CARTESIAN_POINT ( 'NONE',  ( -26.13109729691315053, -24.94783878638828867, 4.221025441685607227 ) ) ;
#88106=CARTESIAN_POINT ( 'NONE',  ( -110.7941382621162631, -25.26164770502454715, 6.209434163990041888 ) ) ;
#88109=CARTESIAN_POINT ( 'NONE',  ( -79.46066275308743343, -25.26749986018558403, 5.472043613161642561 ) ) ;
#88110=CARTESIAN_POINT ( 'NONE',  ( -21.14637036216210575, 8.611126525438130841, -1.500000000000002220 ) ) ;
#88114=CARTESIAN_POINT ( 'NONE',  ( 22.09666729679958053, 4.251135690456572469, 11.49999999999999645 ) ) ;
#88116=LINE ( 'NONE', #25702, #43276 ) ;
#88117=CARTESIAN_POINT ( 'NONE',  ( -19.92591009635028243, 9.278653061003369729, -1.500000000000002220 ) ) ;
#88118=CARTESIAN_POINT ( 'NONE',  ( -114.5228709571500758, -23.72773821059536914, 11.05748984161097326 ) ) ;
#88119=B_SPLINE_CURVE_WITH_KNOTS ( 'NONE', 3,
 ( #66290, #91094, #91591, #82976 ),
 .UNSPECIFIED., .F., .F.,
 ( 4, 4 ),
 ( 0.5601859395450292656, 0.5691923708171451324 ),
 .UNSPECIFIED. ) ;
#88120=CARTESIAN_POINT ( 'NONE',  ( -111.6272352480785770, -24.15543982623907482, -0.2315651400026575712 ) ) ;
#88121=DIRECTION ( 'NONE',  ( -3.773278334453079618E-23, 0.9999999999976377785, 2.173523156925979975E-06 ) ) ;
#88123=CARTESIAN_POINT ( 'NONE',  ( -48.58197809690042135, -24.51419770103156637, 9.386484678747178734 ) ) ;
#88126=CARTESIAN_POINT ( 'NONE',  ( -104.5228709571500758, -29.50248528299804818, 1.056150453629042030 ) ) ;
#88127=CARTESIAN_POINT ( 'NONE',  ( 10.70087849588422380, -17.49211976490306597, -1.500000000000002220 ) ) ;
#88128=ORIENTED_EDGE ( 'NONE', *, *, #53679, .T. ) ;
#88130=ORIENTED_EDGE ( 'NONE', *, *, #94370, .F. ) ;
#88131=CARTESIAN_POINT ( 'NONE',  ( -50.04740315932213690, -25.31331832774112556, 5.238437981263384557 ) ) ;
#88132=CARTESIAN_POINT ( 'NONE',  ( 23.08992502549420323, -0.8469403905869224980, 11.49999999999998934 ) ) ;
#88133=LINE ( 'NONE', #64318, #26079 ) ;
#88134=CARTESIAN_POINT ( 'NONE',  ( -15.63206872509828571, 12.99414084278249071, -1.500000000000002220 ) ) ;
#88136=ORIENTED_EDGE ( 'NONE', *, *, #87507, .F. ) ;
#88138=CARTESIAN_POINT ( 'NONE',  ( -29.59427457724074984, -24.07687357297128727, 10.23563548314527338 ) ) ;
#88139=CARTESIAN_POINT ( 'NONE',  ( -44.58953762381672448, -24.66019654487199375, 8.947790411086137041 ) ) ;
#88140=CARTESIAN_POINT ( 'NONE',  ( -35.62287095715005592, -23.47593901973091235, -1.443836447539011525 ) ) ;
#88141=ORIENTED_EDGE ( 'NONE', *, *, #95520, .F. ) ;
#88142=CARTESIAN_POINT ( 'NONE',  ( -28.81395509834238311, -24.76880987794397626, 2.889656594307629334 ) ) ;
#88143=DIRECTION ( 'NONE',  ( 0.000000000000000000, -0.9999999999976377785, -2.173523156925979975E-06 ) ) ;
#88145=ORIENTED_EDGE ( 'NONE', *, *, #17346, .F. ) ;
#88146=CARTESIAN_POINT ( 'NONE',  ( -11.59579830748209517, 17.24510332420730663, 11.49999999999998934 ) ) ;
#88147=EDGE_LOOP ( 'NONE', ( #16867, #70647, #74690, #61270 ) ) ;
#88148=CARTESIAN_POINT ( 'NONE',  ( -125.5545359397194147, -24.73486907724918638, 1.287355809206972346 ) ) ;
#88152=CARTESIAN_POINT ( 'NONE',  ( -102.6228709571500559, -23.72747288104442021, -1.053458166803661333 ) ) ;
#88153=ORIENTED_EDGE ( 'NONE', *, *, #50462, .T. ) ;
#88155=CARTESIAN_POINT ( 'NONE',  ( -114.6228709571500701, -23.96127896941633040, -0.6493128931037811524 ) ) ;
#88156=CARTESIAN_POINT ( 'NONE',  ( -28.52287095715005805, -24.48903441264110015, 8.947790432046794251 ) ) ;
#88157=PLANE ( 'NONE',  #48138 ) ;
#88158=CARTESIAN_POINT ( 'NONE',  ( -12.21066354923914865, 18.40238043084326591, 11.49999999999999645 ) ) ;
#88160=CARTESIAN_POINT ( 'NONE',  ( -49.11050743085840509, -25.16124551768960416, 6.935735280119078361 ) ) ;
#88161=CARTESIAN_POINT ( 'NONE',  ( 5.419076944403256491, 21.93356404788375258, -1.500000000000002220 ) ) ;
#88164=ADVANCED_FACE ( 'NONE', ( #40830 ), #64707, .T. ) ;
#88165=CARTESIAN_POINT ( 'NONE',  ( -80.34687923781922336, -25.13069340115295702, 2.947789388436138136 ) ) ;
#88166=VERTEX_POINT ( 'NONE', #95622 ) ;
#88170=CARTESIAN_POINT ( 'NONE',  ( -36.62287095715005592, -24.64965695001467694, 8.947790433994187609 ) ) ;
#88172=CARTESIAN_POINT ( 'NONE',  ( -21.15187133135857422, -0.9709546189074961253, -1.500000000000002220 ) ) ;
#88175=CARTESIAN_POINT ( 'NONE',  ( -126.5228709571500616, -29.50247984919015209, -1.443849546365044922 ) ) ;
#88176=B_SPLINE_CURVE_WITH_KNOTS ( 'NONE', 3,
 ( #14608, #69406, #60807, #54689, #85121, #15112 ),
 .UNSPECIFIED., .F., .F.,
 ( 4, 2, 4 ),
 ( 0.000000000000000000, 0.001381645800452327389, 0.002763291600904654779 ),
 .UNSPECIFIED. ) ;
#88177=CARTESIAN_POINT ( 'NONE',  ( 19.86420646539740176, -9.926203236129387264, -1.500000000000002220 ) ) ;
#88178=CARTESIAN_POINT ( 'NONE',  ( -114.5192691221986507, -23.96119346886881374, -0.6495511937831859317 ) ) ;
#88181=CARTESIAN_POINT ( 'NONE',  ( -88.62287095715004170, -24.65952944569304606, 1.056160979905700570 ) ) ;
#88182=CARTESIAN_POINT ( 'NONE',  ( -104.5562042904834072, -23.47593901973091235, -1.443836447539001089 ) ) ;
#88183=CARTESIAN_POINT ( 'NONE',  ( -41.57990624374743760, -25.19387363311069805, 3.356451906250546457 ) ) ;
#88185=EDGE_CURVE ( 'NONE', #44058, #20835, #86055, .T. ) ;
#88186=CARTESIAN_POINT ( 'NONE',  ( 4.731349760756693890, 18.90081699332259646, 11.49999999999998934 ) ) ;
#88187=CARTESIAN_POINT ( 'NONE',  ( 20.52986552169224410, -6.224258026782483633, -1.500000000000002220 ) ) ;
#88191=CARTESIAN_POINT ( 'NONE',  ( -77.60587273036531997, -23.48783264082476663, -1.443836473390097241 ) ) ;
#88192=CARTESIAN_POINT ( 'NONE',  ( 21.73672277138745201, -6.736064506363727666, -1.500000000000002220 ) ) ;
#88193=VECTOR ( 'NONE', #69093, 1000.000000000000114 ) ;
#88194=EDGE_CURVE ( 'NONE', #7527, #53428, #81216, .T. ) ;
#88195=CARTESIAN_POINT ( 'NONE',  ( -102.5490437353218880, -24.51314013834317151, 0.6176544820404245018 ) ) ;
#88197=CARTESIAN_POINT ( 'NONE',  ( 18.24224480919323810, -7.949361806615760528, 11.49999999999999645 ) ) ;
#88198=CARTESIAN_POINT ( 'NONE',  ( -104.5134582497340858, -24.34968618360934300, 0.1864209137778872205 ) ) ;
#88199=B_SPLINE_CURVE_WITH_KNOTS ( 'NONE', 3,
 ( #75863, #13467, #51554, #98705, #29204, #89607 ),
 .UNSPECIFIED., .F., .F.,
 ( 4, 2, 4 ),
 ( 6.384118695040667903E-06, 0.001386860460836587166, 0.002767336802978133652 ),
 .UNSPECIFIED. ) ;
#88200=CARTESIAN_POINT ( 'NONE',  ( -87.62287095715004170, -24.64965695001468404, 8.947790433994180503 ) ) ;
#88201=CARTESIAN_POINT ( 'NONE',  ( -48.59960436616349710, -23.96119346886880663, -0.6495511937831938143 ) ) ;
#88202=EDGE_LOOP ( 'NONE', ( #9252, #63318, #30240, #86800 ) ) ;
#88203=DIRECTION ( 'NONE',  ( 0.000000000000000000, 2.173523156925980399E-06, -0.9999999999976378895 ) ) ;
#88207=CARTESIAN_POINT ( 'NONE',  ( 21.69746526873944958, -0.4026533170205861545, 11.49999999999998934 ) ) ;
#88208=CARTESIAN_POINT ( 'NONE',  ( -56.65019691563739457, -23.73791477778912196, 11.05961554403170766 ) ) ;
#88209=CARTESIAN_POINT ( 'NONE',  ( -13.24781383850973349, 14.34467480260970795, -1.500000000000002220 ) ) ;
#88211=EDGE_CURVE ( 'NONE', #96640, #25971, #51947, .T. ) ;
#88214=DIRECTION ( 'NONE',  ( 0.9796027006414893545, -4.367567496269849188E-07, 0.2009441437208608627 ) ) ;
#88215=CARTESIAN_POINT ( 'NONE',  ( 19.37909195245082472, -6.530858791768283211, 11.49999999999999645 ) ) ;
#88216=FACE_OUTER_BOUND ( 'NONE', #94880, .T. ) ;
#88217=B_SPLINE_CURVE_WITH_KNOTS ( 'NONE', 3,
 ( #16501, #94637, #9900, #7898, #93625, #56093, #48483, #86025 ),
 .UNSPECIFIED., .F., .F.,
 ( 4, 2, 2, 4 ),
 ( 0.000000000000000000, 0.0002157442958532924937, 0.0004314885917065849875, 0.0008629771834131835274 ),
 .UNSPECIFIED. ) ;
#88219=B_SPLINE_CURVE_WITH_KNOTS ( 'NONE', 3,
 ( #65882, #96804, #66375, #27788 ),
 .UNSPECIFIED., .F., .F.,
 ( 4, 4 ),
 ( 0.000000000000000000, 1.000000000000000000 ),
 .UNSPECIFIED. ) ;
#88220=CARTESIAN_POINT ( 'NONE',  ( -118.6228709571500843, -24.34917612406838217, 0.1852690917426704775 ) ) ;
#88221=ORIENTED_EDGE ( 'NONE', *, *, #29482, .F. ) ;
#88225=CARTESIAN_POINT ( 'NONE',  ( -40.52195330627272796, -23.48786465467240347, 11.44779295918255180 ) ) ;
#88226=CARTESIAN_POINT ( 'NONE',  ( -67.62287095715008434, -23.47596703998600276, 11.44779298504227505 ) ) ;
#88227=VERTEX_POINT ( 'NONE', #13364 ) ;
#88229=CARTESIAN_POINT ( 'NONE',  ( -19.49525799874905729, 12.17417675796824561, 11.49999999999999645 ) ) ;
#88230=CARTESIAN_POINT ( 'NONE',  ( 10.71911242904675987, 20.06137936439360203, -1.500000000000002220 ) ) ;
#88231=CARTESIAN_POINT ( 'NONE',  ( -110.5486993749513687, -24.92592662359561473, 8.075495903018000021 ) ) ;
#88233=CARTESIAN_POINT ( 'NONE',  ( -90.59981940747849194, -23.85016227208580730, -0.8807180028928307536 ) ) ;
#88234=AXIS2_PLACEMENT_3D ( 'NONE', #96307, #33910, #43028 ) ;
#88236=CARTESIAN_POINT ( 'NONE',  ( -89.52287095715010423, -23.96127896942128999, -0.6493128930940261778 ) ) ;
#88237=CARTESIAN_POINT ( 'NONE',  ( -15.13543854793762300, 15.80457324685279374, 11.49999999999998934 ) ) ;
#88239=CARTESIAN_POINT ( 'NONE',  ( -49.62744005137184899, -25.31563369538250541, 5.001783013947322942 ) ) ;
#88241=CARTESIAN_POINT ( 'NONE',  ( -58.59295713816230489, -24.15543982623907127, -0.2315651400026660645 ) ) ;
#88243=CARTESIAN_POINT ( 'NONE',  ( -20.33632446988539400, 1.880062042347348195, 11.49999999999998934 ) ) ;
#88246=CARTESIAN_POINT ( 'NONE',  ( 13.47786528765806580, -18.65256936556403744, 11.49999999999998934 ) ) ;
#88248=ORIENTED_EDGE ( 'NONE', *, *, #7350, .T. ) ;
#88252=CARTESIAN_POINT ( 'NONE',  ( -41.62287095715007013, -24.50321055353804311, 9.387540953477543582 ) ) ;
#88253=CARTESIAN_POINT ( 'NONE',  ( -0.3244385709253747585, -21.36021439428519386, 11.49999999999999645 ) ) ;
#88254=ORIENTED_EDGE ( 'NONE', *, *, #30542, .T. ) ;
#88255=B_SPLINE_CURVE_WITH_KNOTS ( 'NONE', 3,
 ( #54526, #71757, #32680, #47416, #70751, #31682 ),
 .UNSPECIFIED., .F., .F.,
 ( 4, 2, 4 ),
 ( 0.000000000000000000, 0.001380901958385387894, 0.002761803916770775788 ),
 .UNSPECIFIED. ) ;
#88257=CARTESIAN_POINT ( 'NONE',  ( -14.87450875942801254, -16.50811611944624602, 11.49999999999998934 ) ) ;
#88258=CARTESIAN_POINT ( 'NONE',  ( 16.58470376584361361, 12.37529123428901556, 11.49999999999998934 ) ) ;
#88261=CARTESIAN_POINT ( 'NONE',  ( -104.6228709571500559, -29.50247984919015209, -1.443849546365050029 ) ) ;
#88264=CARTESIAN_POINT ( 'NONE',  ( -56.52287095715006870, -24.64898659630367916, 1.056161002820822592 ) ) ;
#88265=ORIENTED_EDGE ( 'NONE', *, *, #51968, .F. ) ;
#88268=CARTESIAN_POINT ( 'NONE',  ( 7.003190781191628744, -19.75400906848480176, -1.500000000000002220 ) ) ;
#88269=CARTESIAN_POINT ( 'NONE',  ( -17.52905966558703454, -13.16386835867055716, 11.49999999999999645 ) ) ;
#88270=AXIS2_PLACEMENT_3D ( 'NONE', #16981, #46439, #69783 ) ;
#88271=EDGE_CURVE ( 'NONE', #19622, #12687, #52948, .T. ) ;
#88272=CARTESIAN_POINT ( 'NONE',  ( -26.71877946146332050, -24.89279912406997752, 7.184564487620880513 ) ) ;
#88274=CARTESIAN_POINT ( 'NONE',  ( 20.52096793114426276, -9.243637136814692568, -1.500000000000002220 ) ) ;
#88275=ADVANCED_FACE ( 'NONE', ( #90995 ), #12865, .T. ) ;
#88276=CARTESIAN_POINT ( 'NONE',  ( -3.961239394588834895, 20.55660451852329018, -1.500000000000002220 ) ) ;
#88277=CARTESIAN_POINT ( 'NONE',  ( -26.09636659181000695, -24.88148713818772961, 4.940287743360734396 ) ) ;
#88278=CARTESIAN_POINT ( 'NONE',  ( -72.52287095715003318, -23.73934037231756022, 11.05740245334329153 ) ) ;
#88279=CARTESIAN_POINT ( 'NONE',  ( -89.22287095715005023, -23.47593901973090169, -1.443836447538996870 ) ) ;
#88280=ORIENTED_EDGE ( 'NONE', *, *, #79675, .T. ) ;
#88281=ORIENTED_EDGE ( 'NONE', *, *, #38069, .T. ) ;
#88284=ORIENTED_EDGE ( 'NONE', *, *, #52482, .T. ) ;
#88285=CARTESIAN_POINT ( 'NONE',  ( 2.027878592902508270, 21.29203748114955985, -1.500000000000002220 ) ) ;
#88288=CARTESIAN_POINT ( 'NONE',  ( -53.62287095715005592, -29.50248528299804818, 1.056150453629033370 ) ) ;
#88289=CARTESIAN_POINT ( 'NONE',  ( -8.250207518706217158, 19.40231308534122689, 11.49999999999998934 ) ) ;
#88290=LINE ( 'NONE', #18761, #56332 ) ;
#88292=CARTESIAN_POINT ( 'NONE',  ( -43.62287095715003460, -23.47596703998600276, 11.44779298504227505 ) ) ;
#88294=CARTESIAN_POINT ( 'NONE',  ( -110.2093792378192063, -25.30161501422653814, 5.585409209247975681 ) ) ;
#88295=CARTESIAN_POINT ( 'NONE',  ( -19.13726171168348245, 10.91495894028074432, -1.500000000000002220 ) ) ;
#88296=ORIENTED_EDGE ( 'NONE', *, *, #21336, .F. ) ;
#88297=CARTESIAN_POINT ( 'NONE',  ( -65.54555213868854935, -24.40133493613049964, 9.663955038902802386 ) ) ;
#88298=B_SPLINE_CURVE_WITH_KNOTS ( 'NONE', 3,
 ( #30999, #61966, #62978, #55358, #71079, #23369 ),
 .UNSPECIFIED., .F., .F.,
 ( 4, 2, 4 ),
 ( 1.570887131795109485E-05, 0.001396322306279764325, 0.002776935741241577573 ),
 .UNSPECIFIED. ) ;
#88299=DIRECTION ( 'NONE',  ( -3.773278334453079030E-23, 0.9999999999976377785, 2.173523156925979128E-06 ) ) ;
#88300=CARTESIAN_POINT ( 'NONE',  ( -78.62287095715009855, -23.96177878511308634, 10.65340807706329862 ) ) ;
#88301=CARTESIAN_POINT ( 'NONE',  ( -28.39364267440558365, -25.14063740019444637, 3.798368663089754182 ) ) ;
#88302=CARTESIAN_POINT ( 'NONE',  ( -84.52287095715007581, -23.48783264082477018, -1.443836473390090802 ) ) ;
#88303=VECTOR ( 'NONE', #17561, 1000.000000000000114 ) ;
#88304=CARTESIAN_POINT ( 'NONE',  ( -102.6228709571500559, -23.47593901973091235, -1.443836447539001089 ) ) ;
#88305=CARTESIAN_POINT ( 'NONE',  ( 9.714863677370791706, 19.00186346016302608, 11.49999999999998934 ) ) ;
#88306=CARTESIAN_POINT ( 'NONE',  ( -81.52287095715004739, -23.72747288104470087, -1.053458166803225904 ) ) ;
#88310=CARTESIAN_POINT ( 'NONE',  ( -22.20892344277460850, -4.061126821146308963, -1.500000000000002220 ) ) ;
#88311=CARTESIAN_POINT ( 'NONE',  ( -123.5562042904833930, -24.64898659630529210, 1.056161002820830142 ) ) ;
#88312=VERTEX_POINT ( 'NONE', #43833 ) ;
#88314=CARTESIAN_POINT ( 'NONE',  ( -70.52287095715007581, -23.47593901973090524, -1.443836447538997092 ) ) ;
#88315=CARTESIAN_POINT ( 'NONE',  ( 11.81298147481671279, -15.83112273922526470, 11.49999999999999645 ) ) ;
#88316=DIRECTION ( 'NONE',  ( 0.000000000000000000, 0.9999999999976377785, 2.173523156925979975E-06 ) ) ;
#88318=ORIENTED_EDGE ( 'NONE', *, *, #47151, .F. ) ;
#88320=CARTESIAN_POINT ( 'NONE',  ( -29.77605907665351737, -24.60094425751508140, 4.091750246108072808 ) ) ;
#88321=CARTESIAN_POINT ( 'NONE',  ( -61.52287095715006870, -23.96177878511308634, 10.65340807706330573 ) ) ;
#88322=CARTESIAN_POINT ( 'NONE',  ( -16.60028029328060128, 13.79055755010687356, 11.49999999999998934 ) ) ;
#88323=CARTESIAN_POINT ( 'NONE',  ( -71.58953762381672448, -23.47596703998600276, 11.44779298504227505 ) ) ;
#88326=CARTESIAN_POINT ( 'NONE',  ( -81.85706362847145101, -25.22784785830409149, 6.463371807680155179 ) ) ;
#88327=EDGE_CURVE ( 'NONE', #12640, #92874, #27616, .T. ) ;
#88328=CARTESIAN_POINT ( 'NONE',  ( -1.996473883165060581, 19.68112600131995293, -1.500000000000002220 ) ) ;
#88330=CARTESIAN_POINT ( 'NONE',  ( 11.01437679584920026, 17.03896688766576517, 11.49999999999999645 ) ) ;
#88333=VECTOR ( 'NONE', #4989, 1000.000000000000114 ) ;
#88335=CARTESIAN_POINT ( 'NONE',  ( -110.6228709571500559, -23.85196035786901803, -0.8779234886474867050 ) ) ;
#88341=CARTESIAN_POINT ( 'NONE',  ( -10.14125802585430947, 17.27231531754821603, 11.49999999999998934 ) ) ;
#88344=EDGE_LOOP ( 'NONE', ( #40947, #34473, #57587, #37711 ) ) ;
#88346=DIRECTION ( 'NONE',  ( -3.773278334453079030E-23, 0.9999999999976377785, 2.173523156925979128E-06 ) ) ;
#88347=CARTESIAN_POINT ( 'NONE',  ( -35.58477060636910494, -24.63355581998387223, 0.9682620441943878831 ) ) ;
#88348=CARTESIAN_POINT ( 'NONE',  ( -63.55620429048337883, -24.64965694238574301, 8.947790433994201820 ) ) ;
#88349=CARTESIAN_POINT ( 'NONE',  ( -105.5228709571500758, -24.91544648472621759, 1.928969306349233914 ) ) ;
#88350=CARTESIAN_POINT ( 'NONE',  ( -103.5228709571501184, -24.34917612406837151, 0.1852690917426557671 ) ) ;
#88352=CARTESIAN_POINT ( 'NONE',  ( -98.87424918762685877, -25.30060005375480969, 6.009289253917325269 ) ) ;
#88354=CARTESIAN_POINT ( 'NONE',  ( 0.8761431260907562857, 20.31601184897261092, -1.500000000000002220 ) ) ;
#88355=B_SPLINE_CURVE_WITH_KNOTS ( 'NONE', 3,
 ( #99249, #84527, #91142, #52587, #45981, #76898 ),
 .UNSPECIFIED., .F., .F.,
 ( 4, 2, 4 ),
 ( 6.384118696481608166E-06, 0.001386860460837311196, 0.002767336802978141025 ),
 .UNSPECIFIED. ) ;
#88356=ORIENTED_EDGE ( 'NONE', *, *, #17465, .F. ) ;
#88357=CARTESIAN_POINT ( 'NONE',  ( -8.048360580058307789, -21.46040670285860230, 11.49999999999998934 ) ) ;
#88359=CARTESIAN_POINT ( 'NONE',  ( -127.5900868930851004, -23.96169478059713853, 10.65365249895716637 ) ) ;
#88361=PLANE ( 'NONE',  #29804 ) ;
#88362=CARTESIAN_POINT ( 'NONE',  ( -49.35312698006249832, -25.26264048826114816, 6.504948644732236218 ) ) ;
#88363=CARTESIAN_POINT ( 'NONE',  ( -86.58953762381671027, -23.47593901973091235, -1.443836447539002865 ) ) ;
#88364=CARTESIAN_POINT ( 'NONE',  ( 20.46717832272283033, -5.532298862796615424, 11.49999999999999645 ) ) ;
#88365=VECTOR ( 'NONE', #83204, 1000.000000000000114 ) ;
#88366=CARTESIAN_POINT ( 'NONE',  ( -20.57447749561850969, 8.151157241358404804, -1.500000000000002220 ) ) ;
#88367=CARTESIAN_POINT ( 'NONE',  ( 14.30100545221680441, -14.83292283143518375, 11.49999999999998934 ) ) ;
#88368=VERTEX_POINT ( 'NONE', #28605 ) ;
#88369=CARTESIAN_POINT ( 'NONE',  ( -41.52885629564732284, -24.65952944569304606, 1.056160979905696351 ) ) ;
#88372=FACE_OUTER_BOUND ( 'NONE', #68613, .T. ) ;
#88373=ORIENTED_EDGE ( 'NONE', *, *, #29330, .F. ) ;
#88374=EDGE_CURVE ( 'NONE', #76871, #91107, #2498, .T. ) ;
#88376=VERTEX_POINT ( 'NONE', #75268 ) ;
#88377=CARTESIAN_POINT ( 'NONE',  ( -111.7814946224345789, -25.29712067403330877, 4.332404411321261861 ) ) ;
#88378=CARTESIAN_POINT ( 'NONE',  ( -28.47997080486860710, -24.34985781594834364, 9.386484685950517104 ) ) ;
#88379=DIRECTION ( 'NONE',  ( -3.773278334453079030E-23, 0.9999999999976377785, 2.173523156925979128E-06 ) ) ;
#88380=CARTESIAN_POINT ( 'NONE',  ( -6.500255983836059848, -19.66680810221124887, -1.500000000000002220 ) ) ;
#88381=CARTESIAN_POINT ( 'NONE',  ( 19.26462925850498920, -9.998780574493274287, 11.49999999999999645 ) ) ;
#88382=ORIENTED_EDGE ( 'NONE', *, *, #14028, .F. ) ;
#88384=CARTESIAN_POINT ( 'NONE',  ( -98.89485989515169706, -25.26150877536736772, 6.039289736180342594 ) ) ;
#88385=CARTESIAN_POINT ( 'NONE',  ( -111.7693513301115900, -25.27516155285008992, 4.137661877063939286 ) ) ;
#88386=CARTESIAN_POINT ( 'NONE',  ( -16.61153998044026991, -15.06042057022924929, -1.500000000000002220 ) ) ;
#88390=ORIENTED_EDGE ( 'NONE', *, *, #28408, .F. ) ;
#88392=PLANE ( 'NONE',  #37781 ) ;
#88393=EDGE_CURVE ( 'NONE', #51301, #58944, #60545, .T. ) ;
#88396=ORIENTED_EDGE ( 'NONE', *, *, #72578, .T. ) ;
#88397=B_SPLINE_CURVE_WITH_KNOTS ( 'NONE', 3,
 ( #21775, #39017, #77566, #52749 ),
 .UNSPECIFIED., .F., .F.,
 ( 4, 4 ),
 ( 0.000000000000000000, 0.0001000000000000028644 ),
 .UNSPECIFIED. ) ;
#88399=CARTESIAN_POINT ( 'NONE',  ( -103.6228709571500985, -23.94994826722517089, -0.6494450866351687557 ) ) ;
#88402=CARTESIAN_POINT ( 'NONE',  ( 6.411417644607832145, 20.24884965431308714, -1.500000000000002220 ) ) ;
#88403=EDGE_LOOP ( 'NONE', ( #10685, #52304, #99958, #95389 ) ) ;
#88404=CARTESIAN_POINT ( 'NONE',  ( -68.62287095715005592, -23.48783264082478439, -1.443836473390067265 ) ) ;
#88405=CARTESIAN_POINT ( 'NONE',  ( 19.17057494584436839, 10.47865234463220396, -1.500000000000002220 ) ) ;
#88406=CARTESIAN_POINT ( 'NONE',  ( -52.51445879613589796, -23.73791477778911840, 11.05961554403171476 ) ) ;
#88407=CARTESIAN_POINT ( 'NONE',  ( -40.75388878839229534, -25.18430879041033421, 3.329423250322895100 ) ) ;
#88409=CARTESIAN_POINT ( 'NONE',  ( -44.52287095715006160, -29.50248528299804818, 1.056150453629031594 ) ) ;
#88410=CARTESIAN_POINT ( 'NONE',  ( 21.88901064076550185, 0.7357440816682787599, -1.500000000000002220 ) ) ;
#88413=EDGE_CURVE ( 'NONE', #14381, #53590, #78660, .T. ) ;
#88414=CARTESIAN_POINT ( 'NONE',  ( -69.62287095715005592, -23.73907113216991149, -1.053371485793230811 ) ) ;
#88415=CARTESIAN_POINT ( 'NONE',  ( -121.5562042904833504, -23.47593901973091235, -1.443836447538997536 ) ) ;
#88416=AXIS2_PLACEMENT_3D ( 'NONE', #36857, #38342, #52084 ) ;
#88419=CARTESIAN_POINT ( 'NONE',  ( -32.52287095715006160, -24.64965694238575011, 8.947790433994207149 ) ) ;
#88420=ORIENTED_EDGE ( 'NONE', *, *, #80597, .F. ) ;
#88421=LINE ( 'NONE', #11785, #88091 ) ;
#88422=CARTESIAN_POINT ( 'NONE',  ( -10.22956868858724100, -23.25619435864494378, 1.633150109380534509 ) ) ;
#88423=CARTESIAN_POINT ( 'NONE',  ( 17.84191302092929021, 11.53353326677314961, -1.500000000000002220 ) ) ;
#88424=DIRECTION ( 'NONE',  ( -3.773278334444167608E-23, 1.000000000000000000, 0.000000000000000000 ) ) ;
#88427=CARTESIAN_POINT ( 'NONE',  ( -68.62715718384154684, -24.51314013834315375, 0.6176544820404133995 ) ) ;
#88428=CARTESIAN_POINT ( 'NONE',  ( -5.694372300836820777, 18.57635362771370424, -1.500000000000002220 ) ) ;
#88429=CARTESIAN_POINT ( 'NONE',  ( -30.47287095715007510, -23.47593906522708451, -1.422904450652597852 ) ) ;
#88431=CARTESIAN_POINT ( 'NONE',  ( 19.03533760385612439, 4.641190475545474037, 11.49999999999999645 ) ) ;
#88433=DIRECTION ( 'NONE',  ( 0.000000000000000000, -2.173523156925980399E-06, 0.9999999999976378895 ) ) ;
#88437=CARTESIAN_POINT ( 'NONE',  ( -89.56218751811385914, -23.48783264082478084, -1.443836473390068598 ) ) ;
#88439=CARTESIAN_POINT ( 'NONE',  ( -83.52287095715006160, -24.65952944569304606, 1.056160979905698794 ) ) ;
#88440=ADVANCED_FACE ( 'NONE', ( #31087 ), #84877, .T. ) ;
#88441=CARTESIAN_POINT ( 'NONE',  ( -81.13115756185166560, -25.24813961791220862, 7.427330389041354231 ) ) ;
#88442=CARTESIAN_POINT ( 'NONE',  ( 18.28535361393070957, 7.309334553982634652, 11.49999999999998934 ) ) ;
#88443=VERTEX_POINT ( 'NONE', #76746 ) ;
#88445=CARTESIAN_POINT ( 'NONE',  ( -88.52287095715006160, -29.50250243563736774, 8.947779886222139822 ) ) ;
#88448=EDGE_CURVE ( 'NONE', #13615, #78754, #29071, .T. ) ;
#88449=ORIENTED_EDGE ( 'NONE', *, *, #58171, .F. ) ;
#88450=PLANE ( 'NONE',  #74245 ) ;
#88451=CARTESIAN_POINT ( 'NONE',  ( -105.6228709571500133, -24.91570333823100469, 8.075032458375549282 ) ) ;
#88452=CARTESIAN_POINT ( 'NONE',  ( -47.61501443379227538, -23.48783264082478084, -1.443836473390071928 ) ) ;
#88453=CARTESIAN_POINT ( 'NONE',  ( -105.6228709571500701, -24.15516710230295772, 10.28746687063725496 ) ) ;
#88454=CARTESIAN_POINT ( 'NONE',  ( -78.92465937840067625, -25.31249729222309242, 5.276660411446114196 ) ) ;
#88456=PLANE ( 'NONE',  #76972 ) ;
#88457=CARTESIAN_POINT ( 'NONE',  ( -2.986242917674419850, -19.73498743542299749, -1.500000000000002220 ) ) ;
#88458=EDGE_CURVE ( 'NONE', #97387, #89410, #93236, .T. ) ;
#88459=CARTESIAN_POINT ( 'NONE',  ( -101.0634058648739426, -25.22418476227237960, 3.513563706143655541 ) ) ;
#88460=CARTESIAN_POINT ( 'NONE',  ( 7.211006999188390942, 18.53272205163514030, -1.500000000000002220 ) ) ;
#88461=ORIENTED_EDGE ( 'NONE', *, *, #56177, .T. ) ;
#88462=CARTESIAN_POINT ( 'NONE',  ( -91.15361000704896810, -25.27880950044357178, 5.947789066507965572 ) ) ;
#88463=CARTESIAN_POINT ( 'NONE',  ( -51.35995362507909334, -25.19762389802447089, 6.693417099905952128 ) ) ;
#88466=CARTESIAN_POINT ( 'NONE',  ( -17.75621389795859884, -10.86975384844714831, 11.49999999999999645 ) ) ;
#88470=CARTESIAN_POINT ( 'NONE',  ( -7.631545101075025705, 21.52643039700453897, 11.49999999999999645 ) ) ;
#88471=AXIS2_PLACEMENT_3D ( 'NONE', #59159, #74859, #5363 ) ;
#88472=VERTEX_POINT ( 'NONE', #96001 ) ;
#88474=CARTESIAN_POINT ( 'NONE',  ( -89.55620429048339304, -23.47596703998600631, 11.44779298504227683 ) ) ;
#88478=CARTESIAN_POINT ( 'NONE',  ( 8.147030896810244727, 18.52525024547675869, 11.49999999999998934 ) ) ;
#88479=CARTESIAN_POINT ( 'NONE',  ( -49.27764846858840997, -25.25176233969420636, 6.145204990682164414 ) ) ;
#88482=VECTOR ( 'NONE', #43547, 1000.000000000000114 ) ;
#88484=VERTEX_POINT ( 'NONE', #48336 ) ;
#88485=CARTESIAN_POINT ( 'NONE',  ( -79.39652874673353722, -25.30017758679730022, 5.617944653114273379 ) ) ;
#88487=CARTESIAN_POINT ( 'NONE',  ( -13.93161493328335432, -14.37010051631055418, -1.500000000000002220 ) ) ;
#88488=CARTESIAN_POINT ( 'NONE',  ( 2.700122536338566359, 20.86363338933649558, 11.49999999999999645 ) ) ;
#88491=CARTESIAN_POINT ( 'NONE',  ( 16.78392297789021015, 14.29496084597832883, 11.49999999999998934 ) ) ;
#88492=CARTESIAN_POINT ( 'NONE',  ( -39.65036112522632550, -25.27806035532287154, 4.754946624924129672 ) ) ;
#88493=DIRECTION ( 'NONE',  ( 0.000000000000000000, -2.173523156925980399E-06, 0.9999999999976378895 ) ) ;
#88494=CARTESIAN_POINT ( 'NONE',  ( -50.02027282914984596, -25.18440113274999703, 3.346181424171986496 ) ) ;
#88495=CARTESIAN_POINT ( 'NONE',  ( -72.58426024455503978, -24.51314013834316796, 0.6176544820404145097 ) ) ;
#88496=CARTESIAN_POINT ( 'NONE',  ( -31.57477479285322630, -24.65952944569304250, 1.056160979905695463 ) ) ;
#88498=ORIENTED_EDGE ( 'NONE', *, *, #99358, .F. ) ;
#88499=EDGE_CURVE ( 'NONE', #65316, #76238, #57958, .T. ) ;
#88501=CARTESIAN_POINT ( 'NONE',  ( -101.1026865405329147, -25.27404666790166132, 2.999872496792844512 ) ) ;
#88503=CARTESIAN_POINT ( 'NONE',  ( -2.888065500968368227, -20.30684875360264741, -1.500000000000002220 ) ) ;
#88507=AXIS2_PLACEMENT_3D ( 'NONE', #29402, #67985, #53759 ) ;
#88508=DIRECTION ( 'NONE',  ( -3.773278334453079618E-23, 0.9999999999976377785, 2.173523156925979975E-06 ) ) ;
#88509=CARTESIAN_POINT ( 'NONE',  ( -21.99995728619510516, 3.820703864638951952, -1.500000000000002220 ) ) ;
#88511=FACE_OUTER_BOUND ( 'NONE', #21472, .T. ) ;
#88516=CARTESIAN_POINT ( 'NONE',  ( 18.01467621842780176, -10.50282939286117667, -1.500000000000002220 ) ) ;
#88518=VERTEX_POINT ( 'NONE', #80782 ) ;
#88520=ORIENTED_EDGE ( 'NONE', *, *, #11217, .F. ) ;
#88522=CARTESIAN_POINT ( 'NONE',  ( -104.5228709571500758, -23.47593901973090524, -1.443836447538996204 ) ) ;
#88523=CARTESIAN_POINT ( 'NONE',  ( -14.90395405082875335, 14.90835605916499418, -1.500000000000002220 ) ) ;
#88524=ORIENTED_EDGE ( 'NONE', *, *, #50704, .T. ) ;
#88525=CARTESIAN_POINT ( 'NONE',  ( -114.6228709571500701, -24.50321055353806798, 9.387540953477525818 ) ) ;
#88526=CARTESIAN_POINT ( 'NONE',  ( -98.62287095715005592, -23.48783264082478439, -1.443836473390061936 ) ) ;
#88527=FACE_OUTER_BOUND ( 'NONE', #49579, .T. ) ;
#88528=CARTESIAN_POINT ( 'NONE',  ( -101.8751956322788317, -25.03152227061655211, 6.541290337622787554 ) ) ;
#88529=CARTESIAN_POINT ( 'NONE',  ( -129.6228709571500985, -24.50321055353806443, 9.387540953477522265 ) ) ;
#88530=CARTESIAN_POINT ( 'NONE',  ( -12.04083774165243881, -18.01462592983040523, -1.500000000000002220 ) ) ;
#88531=CARTESIAN_POINT ( 'NONE',  ( -63.52287095715003318, -23.96177878511308990, 10.65340807706330217 ) ) ;
#88532=CARTESIAN_POINT ( 'NONE',  ( -21.75032768068154354, -4.810781854073628239, 11.49999999999999645 ) ) ;
#88533=ORIENTED_EDGE ( 'NONE', *, *, #44741, .T. ) ;
#88534=EDGE_CURVE ( 'NONE', #100208, #99331, #52099, .T. ) ;
#88535=CARTESIAN_POINT ( 'NONE',  ( -51.34258402508250185, -25.31441820025300871, 5.647562909900377903 ) ) ;
#88538=ORIENTED_EDGE ( 'NONE', *, *, #63019, .T. ) ;
#88539=VECTOR ( 'NONE', #15178, 1000.000000000000114 ) ;
#88540=CARTESIAN_POINT ( 'NONE',  ( -54.22287095715005023, -23.47593901973090169, -1.443836447538997758 ) ) ;
#88542=B_SPLINE_CURVE_WITH_KNOTS ( 'NONE', 3,
 ( #69703, #76783, #681, #92028, #53494, #61606, #62099, #15898, #30627, #15396, #31627, #77289, #85923, #16396 ),
 .UNSPECIFIED., .F., .F.,
 ( 4, 2, 2, 2, 2, 2, 4 ),
 ( 1.411962612463446054E-17, 0.0001878395792908931427, 0.0003756791585817721366, 0.0007513583171634909304, 0.001127037475745209941, 0.001314877055036069338, 0.001502716634326928735 ),
 .UNSPECIFIED. ) ;
#88545=CARTESIAN_POINT ( 'NONE',  ( -49.97401002309579354, -25.30055537004108857, 4.651112704816034338 ) ) ;
#88548=CARTESIAN_POINT ( 'NONE',  ( -105.5228709571501042, -24.52232992886361984, 0.6492154411906025935 ) ) ;
#88549=VERTEX_POINT ( 'NONE', #18871 ) ;
#88551=CARTESIAN_POINT ( 'NONE',  ( -130.5728709571500303, -24.34523335840901126, -0.02865858326839056461 ) ) ;
#88552=CARTESIAN_POINT ( 'NONE',  ( -14.39434090420295220, 17.20869321163716492, -1.500000000000002220 ) ) ;
#88554=ORIENTED_EDGE ( 'NONE', *, *, #97665, .F. ) ;
#88555=LINE ( 'NONE', #18531, #64440 ) ;
#88556=DIRECTION ( 'NONE',  ( 0.000000000000000000, -0.9999999999976377785, -2.173523156925979975E-06 ) ) ;
#88560=CARTESIAN_POINT ( 'NONE',  ( -97.24175277348885515, -25.14064729901805606, 2.712351064733618422 ) ) ;
#88562=CARTESIAN_POINT ( 'NONE',  ( 8.161054176536994831, -17.82452852192863091, 11.49999999999998934 ) ) ;
#88563=PLANE ( 'NONE',  #466 ) ;
#88565=CARTESIAN_POINT ( 'NONE',  ( -19.93307770644097232, -8.117153041090405807, -1.500000000000002220 ) ) ;
#88567=CARTESIAN_POINT ( 'NONE',  ( -70.86754458488196917, -25.12219113017391336, 6.955654535003185757 ) ) ;
#88568=CARTESIAN_POINT ( 'NONE',  ( -101.4426914514699121, -25.19143170071711779, 3.265421627976601293 ) ) ;
#88569=CARTESIAN_POINT ( 'NONE',  ( -121.6228709571500275, -24.66019654487200441, 8.947790411086119278 ) ) ;
#88570=CARTESIAN_POINT ( 'NONE',  ( 18.48385363477634513, -13.70420857335572506, -1.500000000000002220 ) ) ;
#88575=FACE_OUTER_BOUND ( 'NONE', #52080, .T. ) ;
#88576=CARTESIAN_POINT ( 'NONE',  ( 14.11618873683251252, 14.29484301466228047, 11.49999999999999645 ) ) ;
#88582=CARTESIAN_POINT ( 'NONE',  ( -82.52287095715006160, -24.64965694238407323, 8.947790433994198267 ) ) ;
#88583=CARTESIAN_POINT ( 'NONE',  ( -18.79335158860655142, 6.462138572525057967, -1.500000000000002220 ) ) ;
#88585=CARTESIAN_POINT ( 'NONE',  ( 19.47230031930329730, 2.946587627359682493, -1.500000000000002220 ) ) ;
#88587=CARTESIAN_POINT ( 'NONE',  ( -60.62287095715004881, -23.48783264082478439, -1.443836473390068820 ) ) ;
#88589=CARTESIAN_POINT ( 'NONE',  ( -34.62287095715005592, -29.50248528299804818, 1.056150453629029817 ) ) ;
#88591=CARTESIAN_POINT ( 'NONE',  ( 13.18972694569024640, 15.87703813876158598, 11.49999999999999645 ) ) ;
#88592=VECTOR ( 'NONE', #95410, 1000.000000000000114 ) ;
#88593=B_SPLINE_CURVE_WITH_KNOTS ( 'NONE', 3,
 ( #84544, #100245, #16026, #30760, #46000, #76919 ),
 .UNSPECIFIED., .F., .F.,
 ( 4, 2, 4 ),
 ( 6.391158118961561766E-06, 0.001387004593080780291, 0.002767618028042598960 ),
 .UNSPECIFIED. ) ;
#88595=CARTESIAN_POINT ( 'NONE',  ( -120.5163177514428128, -25.00158670708911046, 2.256160236439219702 ) ) ;
#88596=CARTESIAN_POINT ( 'NONE',  ( -18.33335541821337245, -13.34141728429830742, 11.49999999999999645 ) ) ;
#88597=ORIENTED_EDGE ( 'NONE', *, *, #70924, .F. ) ;
#88598=CARTESIAN_POINT ( 'NONE',  ( -53.52287095715006870, -24.65952944569304606, 1.056160979905693686 ) ) ;
#88599=CARTESIAN_POINT ( 'NONE',  ( -97.62543170153185201, -24.51314013834315730, 0.6176544820404147318 ) ) ;
#88600=CARTESIAN_POINT ( 'NONE',  ( -27.26363273317966573, -24.93063624427344038, 8.203482558825996307 ) ) ;
#88602=EDGE_CURVE ( 'NONE', #94221, #27358, #84787, .T. ) ;
#88604=ORIENTED_EDGE ( 'NONE', *, *, #66082, .F. ) ;
#88606=CARTESIAN_POINT ( 'NONE',  ( 4.459850365305920938, 22.40387240153798487, -1.500000000000002220 ) ) ;
#88607=DIRECTION ( 'NONE',  ( -3.773278334444167608E-23, 1.000000000000000000, 0.000000000000000000 ) ) ;
#88608=CARTESIAN_POINT ( 'NONE',  ( -29.52287095715006160, -29.50248528299834305, 1.056150588822498460 ) ) ;
#88609=CARTESIAN_POINT ( 'NONE',  ( -82.64546651821306966, -23.48786465467241058, 11.44779295918254647 ) ) ;
#88611=CARTESIAN_POINT ( 'NONE',  ( -22.07377061809603092, 4.253497373390751513, 11.49999999999999645 ) ) ;
#88612=ORIENTED_EDGE ( 'NONE', *, *, #90005, .T. ) ;
#88613=CARTESIAN_POINT ( 'NONE',  ( -33.62287095715005592, -23.48786465467240347, 11.44779295918255535 ) ) ;
#88614=CARTESIAN_POINT ( 'NONE',  ( -15.43752342082821905, -15.63289427301443801, -1.500000000000002220 ) ) ;
#88618=ORIENTED_EDGE ( 'NONE', *, *, #53572, .T. ) ;
#88621=ORIENTED_EDGE ( 'NONE', *, *, #74726, .T. ) ;
#88623=CARTESIAN_POINT ( 'NONE',  ( -108.5895376238167245, -23.47593901973091235, -1.443836447538999312 ) ) ;
#88624=CARTESIAN_POINT ( 'NONE',  ( 20.49162120248849561, -0.4999214236376636200, 11.49999999999998934 ) ) ;
#88628=VERTEX_POINT ( 'NONE', #48840 ) ;
#88631=CARTESIAN_POINT ( 'NONE',  ( -3.594920434497504758, 22.80983129501555950, 11.49999999999998934 ) ) ;
#88632=CARTESIAN_POINT ( 'NONE',  ( -104.5908904681664637, -24.15620529776628800, 10.23563542870659759 ) ) ;
#88633=CARTESIAN_POINT ( 'NONE',  ( -13.40315722217803973, 15.35114911505495172, -1.500000000000002220 ) ) ;
#88636=CARTESIAN_POINT ( 'NONE',  ( -51.70072539166535108, -25.27314792116673203, 3.987152059579775809 ) ) ;
#88637=VECTOR ( 'NONE', #98000, 1000.000000000000114 ) ;
#88638=B_SPLINE_CURVE_WITH_KNOTS ( 'NONE', 3,
 ( #58721, #33888, #49132, #89673 ),
 .UNSPECIFIED., .F., .F.,
 ( 4, 4 ),
 ( 0.1989019938671915955, 0.1999027409079570106 ),
 .UNSPECIFIED. ) ;
#88639=CARTESIAN_POINT ( 'NONE',  ( -105.5487342842852030, -24.73486907724918993, 1.287355809206962576 ) ) ;
#88640=CARTESIAN_POINT ( 'NONE',  ( -111.6228709571500843, -23.47596703998600631, 11.44779298504227860 ) ) ;
#88641=VERTEX_POINT ( 'NONE', #27497 ) ;
#88642=CARTESIAN_POINT ( 'NONE',  ( -29.23473450784903704, -25.21532131873518878, 4.453842557699799976 ) ) ;
#88643=CARTESIAN_POINT ( 'NONE',  ( -60.25625423781919210, -25.21083105912961742, 3.409327675794635581 ) ) ;
#88644=VERTEX_POINT ( 'NONE', #67560 ) ;
#88645=CARTESIAN_POINT ( 'NONE',  ( -20.76960556195881225, -0.3855258213679747525, 11.49999999999998934 ) ) ;
#88646=ADVANCED_FACE ( 'NONE', ( #43226 ), #59951, .T. ) ;
#88647=VERTEX_POINT ( 'NONE', #4157 ) ;
#88648=CARTESIAN_POINT ( 'NONE',  ( -109.5228709571500616, -23.48786465467242479, 11.44779295918253936 ) ) ;
#88650=EDGE_CURVE ( 'NONE', #18719, #21744, #14517, .T. ) ;
#88651=CARTESIAN_POINT ( 'NONE',  ( -129.6228709571500417, -24.64898659630367916, 1.056161002820834804 ) ) ;
#88652=CARTESIAN_POINT ( 'NONE',  ( -51.28102184251170570, -25.30566280108310551, 5.070271677697943957 ) ) ;
#88653=EDGE_LOOP ( 'NONE', ( #40466, #98104, #48196, #18143 ) ) ;
#88655=CARTESIAN_POINT ( 'NONE',  ( -79.58953762381672448, -24.65952944569304250, 1.056160979905692354 ) ) ;
#88657=CARTESIAN_POINT ( 'NONE',  ( -70.39323859381175907, -25.24515042351162819, 5.314174096928971913 ) ) ;
#88658=CARTESIAN_POINT ( 'NONE',  ( -2.767897998228395551, 21.91458177938747909, 11.49999999999999645 ) ) ;
#88659=ORIENTED_EDGE ( 'NONE', *, *, #78875, .T. ) ;
#88660=EDGE_CURVE ( 'NONE', #99862, #6550, #82763, .T. ) ;
#88661=CARTESIAN_POINT ( 'NONE',  ( -103.5221972675466731, -23.48783264082477018, -1.443836473390091246 ) ) ;
#88662=CARTESIAN_POINT ( 'NONE',  ( 21.71239400539012721, -6.292901409244172406, 11.49999999999998934 ) ) ;
#88663=VECTOR ( 'NONE', #15879, 1000.000000000000114 ) ;
#88664=EDGE_CURVE ( 'NONE', #23202, #31248, #79943, .T. ) ;
#88666=VERTEX_POINT ( 'NONE', #89885 ) ;
#88667=ORIENTED_EDGE ( 'NONE', *, *, #68614, .F. ) ;
#88668=AXIS2_PLACEMENT_3D ( 'NONE', #59972, #90907, #13764 ) ;
#88670=B_SPLINE_CURVE_WITH_KNOTS ( 'NONE', 3,
 ( #12514, #4913, #29738, #36359, #67315, #35858 ),
 .UNSPECIFIED., .F., .F.,
 ( 4, 2, 4 ),
 ( 6.391158118959990520E-06, 0.001387004593080782460, 0.002767618028042605031 ),
 .UNSPECIFIED. ) ;
#88672=ORIENTED_EDGE ( 'NONE', *, *, #3327, .F. ) ;
#88673=CARTESIAN_POINT ( 'NONE',  ( -17.67215177357914513, -11.65580189297658897, -1.500000000000002220 ) ) ;
#88676=CARTESIAN_POINT ( 'NONE',  ( 10.93216147639808611, 19.43004700418156361, -1.500000000000002220 ) ) ;
#88677=CARTESIAN_POINT ( 'NONE',  ( -88.88918693012689687, -29.50249591506787894, 5.947779886229223045 ) ) ;
#88681=VECTOR ( 'NONE', #56745, 1000.000000000000227 ) ;
#88682=CARTESIAN_POINT ( 'NONE',  ( -36.55285608143805121, -23.96169478059712432, 10.65365249895718591 ) ) ;
#88683=CARTESIAN_POINT ( 'NONE',  ( -126.5228709571500616, -24.64898659630368627, 1.056161002820834804 ) ) ;
#88685=CARTESIAN_POINT ( 'NONE',  ( 2.628080361126900133, -19.32819128710564272, -1.500000000000002220 ) ) ;
#88686=CARTESIAN_POINT ( 'NONE',  ( 21.15477495681221143, 3.540436534888726783, -1.500000000000002220 ) ) ;
#88687=CARTESIAN_POINT ( 'NONE',  ( -26.15505896238250472, -24.92774839236926709, 2.424162040430986043 ) ) ;
#88688=DIRECTION ( 'NONE',  ( -0.000000000000000000, 2.173523156925979552E-06, -0.9999999999976378895 ) ) ;
#88689=CARTESIAN_POINT ( 'NONE',  ( -77.64259777044621558, -23.73766607897670156, -1.055555164236459564 ) ) ;
#88690=B_SPLINE_CURVE_WITH_KNOTS ( 'NONE', 3,
 ( #24117, #55088, #33744, #25627, #56599, #8900 ),
 .UNSPECIFIED., .F., .F.,
 ( 4, 2, 4 ),
 ( 0.000000000000000000, 0.001380901958385389412, 0.002761803916770778824 ),
 .UNSPECIFIED. ) ;
#88691=CARTESIAN_POINT ( 'NONE',  ( -12.51292883401962541, 18.98408452820241266, -1.500000000000002220 ) ) ;
#88695=CARTESIAN_POINT ( 'NONE',  ( -98.50939101541317200, -24.51314013834315020, 0.6176544820404104019 ) ) ;
#88697=CARTESIAN_POINT ( 'NONE',  ( -19.25010300378637851, 5.133817055790010464, 11.49999999999999645 ) ) ;
#88698=CARTESIAN_POINT ( 'NONE',  ( -104.6353677949941954, -23.48783264082477373, -1.443836473390085917 ) ) ;
#88703=CARTESIAN_POINT ( 'NONE',  ( -89.81226385320383088, -29.50249917535260380, 7.447779886225679213 ) ) ;
#88704=CARTESIAN_POINT ( 'NONE',  ( 21.66353188042378974, 1.267531592894010739, 11.49999999999998934 ) ) ;
#88705=CARTESIAN_POINT ( 'NONE',  ( -84.52287095715011844, -23.96177878511309345, 10.65340807706330217 ) ) ;
#88706=CARTESIAN_POINT ( 'NONE',  ( -18.49313839071750820, -6.238557295281221826, -1.500000000000002220 ) ) ;
#88708=ORIENTED_EDGE ( 'NONE', *, *, #63106, .T. ) ;
#88711=CARTESIAN_POINT ( 'NONE',  ( -20.33632446988539400, 1.880062042347348195, 11.49999999999999645 ) ) ;
#88714=EDGE_CURVE ( 'NONE', #38179, #12874, #20354, .T. ) ;
#88717=CARTESIAN_POINT ( 'NONE',  ( -39.46304919600096639, -25.18431026911589754, 4.009749832163960193 ) ) ;
#88719=CARTESIAN_POINT ( 'NONE',  ( -32.07722060962684196, -24.87479601683932984, 8.247789944617052171 ) ) ;
#88723=VECTOR ( 'NONE', #42619, 1000.000000000000114 ) ;
#88725=EDGE_CURVE ( 'NONE', #12246, #31523, #94499, .T. ) ;
#88726=B_SPLINE_CURVE_WITH_KNOTS ( 'NONE', 3,
 ( #42394, #94650, #95658, #32749, #96648, #41884 ),
 .UNSPECIFIED., .F., .F.,
 ( 4, 2, 4 ),
 ( 0.000000000000000000, 0.001380901958385392448, 0.002761803916770784895 ),
 .UNSPECIFIED. ) ;
#88727=CARTESIAN_POINT ( 'NONE',  ( 8.272623322502495213, 21.45567517505680044, 11.49999999999999645 ) ) ;
#88728=CARTESIAN_POINT ( 'NONE',  ( 12.23086119556625206, 19.17791753167082192, -1.500000000000002220 ) ) ;
#88730=B_SPLINE_SURFACE_WITH_KNOTS ( 'NONE', 3, 1, ( 
 ( #39494, #63353 ),
 ( #92763, #8541 ),
 ( #47614, #48623 ),
 ( #423, #25259 ),
 ( #17653, #78533 ),
 ( #38985, #62339 ),
 ( #40498, #8034 ),
 ( #9037, #39990 ),
 ( #15646, #71453 ),
 ( #86660, #70950 ),
 ( #93265, #70444 ),
 ( #69935, #79549 ),
 ( #54729, #1439 ),
 ( #85664, #56238 ),
 ( #16144, #47116 ),
 ( #17149, #87163 ),
 ( #32376, #94269 ),
 ( #24753, #10039 ),
 ( #40999, #931 ) ),
 .UNSPECIFIED., .F., .F., .F.,
 ( 4, 1, 1, 1, 1, 1, 1, 1, 1, 1, 1, 1, 1, 1, 1, 1, 4 ),
 ( 2, 2 ),
 ( 0.000000000000000000, 0.07855643335270047489, 0.1528628401420922822, 0.2235596934382872158, 0.2903749439782072894, 0.3554030728222035140, 0.4182911570440911442, 0.4803885637756447058, 0.5430726152062789192, 0.6049239444620954087, 0.6643983091132997787, 0.7219425547367019913, 0.7783748910546737232, 0.8338299406509398493, 0.8888612363188844734, 0.9440889395778866433, 1.000000000000000000 ),
 ( 0.000000000000000000, 1.000000000000000000 ),
 .UNSPECIFIED. ) ;
#88732=CARTESIAN_POINT ( 'NONE',  ( -90.59507163750394909, -24.15503026093915651, -0.2815557561904460382 ) ) ;
#88733=EDGE_CURVE ( 'NONE', #38686, #44615, #12187, .T. ) ;
#88734=AXIS2_PLACEMENT_3D ( 'NONE', #39875, #15029, #30254 ) ;
#88735=CARTESIAN_POINT ( 'NONE',  ( -124.9228709571500531, -23.47593901973090524, -1.443836447538996204 ) ) ;
#88736=CARTESIAN_POINT ( 'NONE',  ( -44.62287095715004881, -23.48783264082478084, -1.443836473390072150 ) ) ;
#88737=CARTESIAN_POINT ( 'NONE',  ( -19.96805355746080934, -8.928269573510897672, 11.49999999999998934 ) ) ;
#88738=CARTESIAN_POINT ( 'NONE',  ( -74.52287095715007581, -24.64898659630528854, 1.056161002820824368 ) ) ;
#88740=CARTESIAN_POINT ( 'NONE',  ( -120.6228709571500417, -24.99132157543166954, 2.256160258750667502 ) ) ;
#88742=ORIENTED_EDGE ( 'NONE', *, *, #13451, .T. ) ;
#88743=CARTESIAN_POINT ( 'NONE',  ( 12.15263457413992576, -16.39098610538439615, 11.49999999999998934 ) ) ;
#88747=ORIENTED_EDGE ( 'NONE', *, *, #40823, .F. ) ;
#88749=ADVANCED_FACE ( 'NONE', ( #29973 ), #62440, .F. ) ;
#88750=CARTESIAN_POINT ( 'NONE',  ( -20.90396053131702914, -9.656267258341529214, -1.500000000000002220 ) ) ;
#88751=CARTESIAN_POINT ( 'NONE',  ( -60.62287095715004881, -29.50247984919015209, -1.443849546365056913 ) ) ;
#88752=CARTESIAN_POINT ( 'NONE',  ( -19.56588111578679090, -4.897929960003377658, -1.500000000000002220 ) ) ;
#88753=ORIENTED_EDGE ( 'NONE', *, *, #63727, .F. ) ;
#88754=CARTESIAN_POINT ( 'NONE',  ( -67.62287095715002749, -24.35013146730203815, 9.818937971375108376 ) ) ;
#88756=CARTESIAN_POINT ( 'NONE',  ( -101.5228709571500758, -23.48786465467241769, 11.44779295918254114 ) ) ;
#88757=CARTESIAN_POINT ( 'NONE',  ( -53.60570705064769470, -23.73791477778911485, 11.05961554403170766 ) ) ;
#88758=CARTESIAN_POINT ( 'NONE',  ( 21.01207135711032237, 3.775690236426352264, 11.49999999999999645 ) ) ;
#88759=ORIENTED_EDGE ( 'NONE', *, *, #83495, .T. ) ;
#88762=CARTESIAN_POINT ( 'NONE',  ( 22.17158117043571863, -1.905908075979310334, 11.49999999999998934 ) ) ;
#88763=CARTESIAN_POINT ( 'NONE',  ( -19.97286373971314433, -5.326668811655218327, 11.49999999999998934 ) ) ;
#88768=ORIENTED_EDGE ( 'NONE', *, *, #58101, .F. ) ;
#88769=CARTESIAN_POINT ( 'NONE',  ( -78.62287095715005592, -23.47593901973091235, -1.443836447539004642 ) ) ;
#88771=ORIENTED_EDGE ( 'NONE', *, *, #69014, .F. ) ;
#88772=CARTESIAN_POINT ( 'NONE',  ( -50.21186637932700592, -25.10935128237196068, 2.837931291232954401 ) ) ;
#88773=CARTESIAN_POINT ( 'NONE',  ( -18.75169668496848985, 9.291489096422434812, -1.500000000000002220 ) ) ;
#88774=CARTESIAN_POINT ( 'NONE',  ( -21.18249553426131015, -5.656070447573528170, 11.49999999999999645 ) ) ;
#88775=EDGE_CURVE ( 'NONE', #43186, #7527, #10939, .T. ) ;
#88776=CARTESIAN_POINT ( 'NONE',  ( -73.62685146875698194, -24.51419770103157347, 9.386484678747175181 ) ) ;
#88777=CARTESIAN_POINT ( 'NONE',  ( -21.69688529672534827, 6.072505851105969299, -1.500000000000002220 ) ) ;
#88778=CARTESIAN_POINT ( 'NONE',  ( 5.463070048063013218, -20.23478146675526190, -1.500000000000002220 ) ) ;
#88780=CARTESIAN_POINT ( 'NONE',  ( -26.33488822642538452, -24.97067133876658929, 6.524121684135936405 ) ) ;
#88784=ORIENTED_EDGE ( 'NONE', *, *, #15797, .T. ) ;
#88788=CARTESIAN_POINT ( 'NONE',  ( -94.62287095715005592, -23.47593901973091235, -1.443836447539002865 ) ) ;
#88790=CARTESIAN_POINT ( 'NONE',  ( 16.48747857468482891, 13.79107804547330929, -1.500000000000002220 ) ) ;
#88791=EDGE_CURVE ( 'NONE', #26599, #13615, #48511, .T. ) ;
#88792=ORIENTED_EDGE ( 'NONE', *, *, #95705, .F. ) ;
#88794=CARTESIAN_POINT ( 'NONE',  ( 5.994809752082427501, 20.21905721239408393, 11.49999999999998934 ) ) ;
#88796=CARTESIAN_POINT ( 'NONE',  ( -64.65370588801016538, -23.48783264082477018, -1.443836473390096353 ) ) ;
#88797=CARTESIAN_POINT ( 'NONE',  ( -50.67080941327229482, -23.48786465467240347, 11.44779295918255002 ) ) ;
#88798=CARTESIAN_POINT ( 'NONE',  ( -101.5146404698777900, -24.15543982623907482, -0.2315651400026588758 ) ) ;
#88800=CARTESIAN_POINT ( 'NONE',  ( -10.28628152547328511, -19.52461415289770130, -1.500000000000002220 ) ) ;
#88802=CARTESIAN_POINT ( 'NONE',  ( -116.6243012131220240, -24.51314013834316086, 0.6176544820404278324 ) ) ;
#88803=FACE_OUTER_BOUND ( 'NONE', #47623, .T. ) ;
#88804=CARTESIAN_POINT ( 'NONE',  ( -40.49165087243459737, -25.27956071481186839, 5.543942911029563270 ) ) ;
#88806=CARTESIAN_POINT ( 'NONE',  ( -29.85657701416236520, -24.77034389998055985, 1.590605884330587916 ) ) ;
#88808=CARTESIAN_POINT ( 'NONE',  ( 18.61059577090848549, -10.47110149595715711, -1.500000000000002220 ) ) ;
#88809=CARTESIAN_POINT ( 'NONE',  ( -70.35231919018949043, -25.31467665484316854, 4.853663865497455987 ) ) ;
#88810=CARTESIAN_POINT ( 'NONE',  ( -89.80335865247931793, -25.31768024997816724, 4.634761245912266681 ) ) ;
#88811=CARTESIAN_POINT ( 'NONE',  ( -64.58768515828387535, -24.35071581493543391, 9.817618358456023486 ) ) ;
#88812=CARTESIAN_POINT ( 'NONE',  ( -80.77696901427715659, -25.12955870785331669, 7.063884950381287275 ) ) ;
#88813=CARTESIAN_POINT ( 'NONE',  ( 21.16457415087624128, -7.944649954575952577, -1.500000000000002220 ) ) ;
#88814=B_SPLINE_SURFACE_WITH_KNOTS ( 'NONE', 3, 3, ( 
 ( #51715, #75031, #76030, #36984 ),
 ( #91756, #84149, #82655, #66473 ),
 ( #98873, #97870, #83148, #13630 ),
 ( #44601, #6031, #67947, #97388 ),
 ( #43109, #6535, #82158, #37484 ),
 ( #68436, #29866, #60839, #22235 ),
 ( #27873, #12642, #43605, #15640 ) ),
 .UNSPECIFIED., .F., .F., .F.,
 ( 4, 3, 4 ),
 ( 4, 4 ),
 ( 0.0004766839783814535341, 0.1029713700210890953, 0.2054660560637967259 ),
 ( 0.6396567149882574910, 0.6409645759772608642 ),
 .UNSPECIFIED. ) ;
#88815=PLANE ( 'NONE',  #97670 ) ;
#88816=ORIENTED_EDGE ( 'NONE', *, *, #75741, .F. ) ;
#88819=CARTESIAN_POINT ( 'NONE',  ( -16.30015253881794379, -11.17962500214296639, 11.49999999999999645 ) ) ;
#88821=CARTESIAN_POINT ( 'NONE',  ( -96.52287095715007581, -23.47593901973090524, -1.443836447538996648 ) ) ;
#88824=CARTESIAN_POINT ( 'NONE',  ( -80.64675904551154417, -25.21083105912962807, 3.409327675794629808 ) ) ;
#88825=CARTESIAN_POINT ( 'NONE',  ( -110.5895376238167245, -23.47593901973091235, -1.443836447538999312 ) ) ;
#88826=CARTESIAN_POINT ( 'NONE',  ( -113.5228709571500616, -24.64898659630368627, 1.056161002820831474 ) ) ;
#88827=CARTESIAN_POINT ( 'NONE',  ( -19.28869470675124731, 9.786980993800005635, 11.49999999999998934 ) ) ;
#88828=DIRECTION ( 'NONE',  ( 0.000000000000000000, -2.173523156925980399E-06, 0.9999999999976378895 ) ) ;
#88830=CARTESIAN_POINT ( 'NONE',  ( -66.52287095715006160, -23.96177878511308990, 10.65340807706329684 ) ) ;
#88831=CARTESIAN_POINT ( 'NONE',  ( -92.58953762381671027, -23.48783264082479150, -1.443836473390063713 ) ) ;
#88833=CARTESIAN_POINT ( 'NONE',  ( -10.52764212615999639, 16.74383705166681580, -1.500000000000002220 ) ) ;
#88834=ORIENTED_EDGE ( 'NONE', *, *, #43721, .T. ) ;
#88835=CARTESIAN_POINT ( 'NONE',  ( -8.208445925564873846, -18.52556626786687488, 11.49999999999999645 ) ) ;
#88836=CARTESIAN_POINT ( 'NONE',  ( -112.6228709571501412, -24.35013146730204170, 9.818937971375106599 ) ) ;
#88837=VECTOR ( 'NONE', #25865, 1000.000000000000114 ) ;
#88839=VERTEX_POINT ( 'NONE', #45711 ) ;
#88842=CARTESIAN_POINT ( 'NONE',  ( -59.62287095715004881, -29.50250243563736774, 8.947779886222145151 ) ) ;
#88845=CARTESIAN_POINT ( 'NONE',  ( -47.62287095715004881, -29.50250243563736774, 8.947779886222146928 ) ) ;
#88848=CARTESIAN_POINT ( 'NONE',  ( 17.53424486177994623, -9.724335930198575895, -1.500000000000002220 ) ) ;
#88850=CARTESIAN_POINT ( 'NONE',  ( -51.62287095715005592, -23.47596703998600631, 11.44779298504227505 ) ) ;
#88852=ADVANCED_FACE ( 'NONE', ( #46206 ), #15751, .T. ) ;
#88853=EDGE_CURVE ( 'NONE', #51364, #88644, #22930, .T. ) ;
#88854=CARTESIAN_POINT ( 'NONE',  ( -73.62287095715009855, -23.95044443724992433, 10.65354141964649948 ) ) ;
#88855=PLANE ( 'NONE',  #13702 ) ;
#88857=PLANE ( 'NONE',  #82092 ) ;
#88858=CARTESIAN_POINT ( 'NONE',  ( -73.56460343122959955, -23.48783264082477018, -1.443836473390094355 ) ) ;
#88860=B_SPLINE_CURVE_WITH_KNOTS ( 'NONE', 3,
 ( #77184, #7690, #36643, #67610, #98528, #60000, #90929, #13792 ),
 .UNSPECIFIED., .F., .F.,
 ( 4, 2, 2, 4 ),
 ( -0.001224873891641426078, -0.0002244903592271097967, 0.0007758931731872064849, 0.002776660238015834711 ),
 .UNSPECIFIED. ) ;
#88861=CARTESIAN_POINT ( 'NONE',  ( -93.52287095715006160, -24.64898659630368272, 1.056161002820827921 ) ) ;
#88863=CARTESIAN_POINT ( 'NONE',  ( -18.82647582233506611, 7.659846263794035437, -1.500000000000002220 ) ) ;
#88864=ORIENTED_EDGE ( 'NONE', *, *, #6148, .T. ) ;
#88865=EDGE_CURVE ( 'NONE', #15988, #62185, #66677, .T. ) ;
#88866=CARTESIAN_POINT ( 'NONE',  ( -0.4961427919413599064, 22.93664481792237453, 11.49999999999998934 ) ) ;
#88867=CARTESIAN_POINT ( 'NONE',  ( -32.59412366074091949, -24.15543982623907127, -0.2315651400026567941 ) ) ;
#88870=CARTESIAN_POINT ( 'NONE',  ( -76.52287095715007581, -24.64898659630528854, 1.056161002820826145 ) ) ;
#88871=EDGE_CURVE ( 'NONE', #73153, #58829, #93367, .T. ) ;
#88873=CARTESIAN_POINT ( 'NONE',  ( -19.98373207111551508, 7.008865001458166155, 11.49999999999999645 ) ) ;
#88874=CARTESIAN_POINT ( 'NONE',  ( 9.107982344273736430, -20.20341329189913537, 11.49999999999998934 ) ) ;
#88875=CARTESIAN_POINT ( 'NONE',  ( 11.80677006232881254, 16.86875346446678137, -1.500000000000002220 ) ) ;
#88877=CARTESIAN_POINT ( 'NONE',  ( -41.56077753939339203, -23.73766607897670866, -1.055555164236442023 ) ) ;
#88879=CARTESIAN_POINT ( 'NONE',  ( -54.48738976181418536, -24.65952944569304606, 1.056160979905696573 ) ) ;
#88883=ORIENTED_EDGE ( 'NONE', *, *, #80705, .F. ) ;
#88885=CARTESIAN_POINT ( 'NONE',  ( -28.54452471549034698, -23.99578543409190701, 10.23563545308467226 ) ) ;
#88886=CARTESIAN_POINT ( 'NONE',  ( -64.52287095715006160, -23.48786465467241769, 11.44779295918254824 ) ) ;
#88887=CARTESIAN_POINT ( 'NONE',  ( 2.040502595053849788, 20.68626321094233944, -1.500000000000002220 ) ) ;
#88888=CARTESIAN_POINT ( 'NONE',  ( -16.45766974254678061, 14.19212061201335473, 11.49999999999999645 ) ) ;
#88890=CARTESIAN_POINT ( 'NONE',  ( -69.65500149314945588, -25.14915147881072244, 2.995210818656448115 ) ) ;
#88891=CARTESIAN_POINT ( 'NONE',  ( -115.5133559575585451, -25.00158670708910691, 2.256160236439219258 ) ) ;
#88892=CARTESIAN_POINT ( 'NONE',  ( 21.53444271425275858, 6.169869319618734416, -1.500000000000002220 ) ) ;
#88893=AXIS2_PLACEMENT_3D ( 'NONE', #95318, #87708, #80091 ) ;
#88895=CARTESIAN_POINT ( 'NONE',  ( -124.5228709571500900, -23.48783264082477373, -1.443836473390085029 ) ) ;
#88896=CARTESIAN_POINT ( 'NONE',  ( -71.62287095715005592, -24.34917612406837861, 0.1852690917426617345 ) ) ;
#88897=ORIENTED_EDGE ( 'NONE', *, *, #40497, .F. ) ;
#88898=CARTESIAN_POINT ( 'NONE',  ( -45.52287095715006160, -24.99132157543083821, 2.256160258750667502 ) ) ;
#88899=CARTESIAN_POINT ( 'NONE',  ( -77.55620429048339304, -23.47596703998600276, 11.44779298504227683 ) ) ;
#88900=ORIENTED_EDGE ( 'NONE', *, *, #5208, .F. ) ;
#88903=CARTESIAN_POINT ( 'NONE',  ( -103.6228709571500559, -23.47593901973091235, -1.443836447539001089 ) ) ;
#88904=ORIENTED_EDGE ( 'NONE', *, *, #46979, .F. ) ;
#88905=CARTESIAN_POINT ( 'NONE',  ( -13.59518820711925358, -16.35513075224449864, -1.500000000000002220 ) ) ;
#88906=ORIENTED_EDGE ( 'NONE', *, *, #1812, .F. ) ;
#88908=CARTESIAN_POINT ( 'NONE',  ( -9.754611696910345131, 19.53525426502628548, 11.49999999999998934 ) ) ;
#88909=CARTESIAN_POINT ( 'NONE',  ( -52.65922807883639223, -23.48786465467240703, 11.44779295918255180 ) ) ;
#88910=CARTESIAN_POINT ( 'NONE',  ( 2.978076788109338402, -22.46882643481310282, -1.500000000000002220 ) ) ;
#88912=CARTESIAN_POINT ( 'NONE',  ( -49.52287095715005449, -24.51387760970724727, 9.387446482453427166 ) ) ;
#88913=CARTESIAN_POINT ( 'NONE',  ( -21.85961425739535358, 0.8689724601130633941, -1.500000000000002220 ) ) ;
#88916=CARTESIAN_POINT ( 'NONE',  ( -65.62287095715005592, -23.48783264082478084, -1.443836473390067265 ) ) ;
#88917=CARTESIAN_POINT ( 'NONE',  ( -49.21454750704995007, -25.26337504824086722, 7.069183330828471057 ) ) ;
#88918=ORIENTED_EDGE ( 'NONE', *, *, #39711, .F. ) ;
#88919=CARTESIAN_POINT ( 'NONE',  ( -32.52287095715006160, -24.33927499327854349, 9.819080762295817166 ) ) ;
#88921=ORIENTED_EDGE ( 'NONE', *, *, #68881, .F. ) ;
#88922=CARTESIAN_POINT ( 'NONE',  ( -128.5562042904834357, -23.47596703998600631, 11.44779298504227683 ) ) ;
#88924=CARTESIAN_POINT ( 'NONE',  ( -19.44786352930952233, -8.617208915446557427, -1.500000000000002220 ) ) ;
#88926=CARTESIAN_POINT ( 'NONE',  ( -26.30595710371889950, -24.75186218799666804, 3.418819366253220693 ) ) ;
#88927=CARTESIAN_POINT ( 'NONE',  ( -85.60108179270328321, -23.85016227208579664, -0.8807180028928370819 ) ) ;
#88928=CARTESIAN_POINT ( 'NONE',  ( -68.55393007522499715, -23.96119346886880663, -0.6495511937832112448 ) ) ;
#88929=CARTESIAN_POINT ( 'NONE',  ( -117.5579608062422921, -23.48786465467241769, 11.44779295918253581 ) ) ;
#88930=ORIENTED_EDGE ( 'NONE', *, *, #35373, .F. ) ;
#88931=CARTESIAN_POINT ( 'NONE',  ( 8.254404603115069960, -17.72612730319335839, 11.49999999999999645 ) ) ;
#88933=CARTESIAN_POINT ( 'NONE',  ( -79.34687923781920915, -25.26778825442007559, 5.960409282772108241 ) ) ;
#88935=CARTESIAN_POINT ( 'NONE',  ( -104.5228709571500758, -24.64898659630529565, 1.056161002820829697 ) ) ;
#88936=CARTESIAN_POINT ( 'NONE',  ( -99.63322708413970474, -25.25095836864358745, 5.473920322365175117 ) ) ;
#88937=CARTESIAN_POINT ( 'NONE',  ( -90.62287095715004170, -23.47593901973091235, -1.443836447539002865 ) ) ;
#88938=CARTESIAN_POINT ( 'NONE',  ( -60.52287095715009002, -24.15431212366390312, -0.2830839119429246487 ) ) ;
#88939=CARTESIAN_POINT ( 'NONE',  ( 3.778003860535555702, 19.31821889988591323, -1.500000000000002220 ) ) ;
#88940=ORIENTED_EDGE ( 'NONE', *, *, #26241, .F. ) ;
#88945=ORIENTED_EDGE ( 'NONE', *, *, #88327, .T. ) ;
#88946=CARTESIAN_POINT ( 'NONE',  ( -99.52764846858842418, -25.26416398485831749, 3.999772271414141489 ) ) ;
#88948=CARTESIAN_POINT ( 'NONE',  ( -84.62287095715005592, -24.66019654487199730, 8.947790411086128159 ) ) ;
#88949=CARTESIAN_POINT ( 'NONE',  ( -97.50710338837967583, -24.66019654487199730, 8.947790411086115725 ) ) ;
#88950=CARTESIAN_POINT ( 'NONE',  ( -47.62287095715004881, -23.48786465467240703, 11.44779295918255180 ) ) ;
#88955=B_SPLINE_CURVE_WITH_KNOTS ( 'NONE', 3,
 ( #94548, #65138, #18925, #10822, #26554, #88453, #18433, #27050 ),
 .UNSPECIFIED., .F., .F.,
 ( 4, 2, 2, 4 ),
 ( -0.001224554619866345413, -0.0002241820295893650998, 0.0007761905606876152129, 0.002776935741241572369 ),
 .UNSPECIFIED. ) ;
#88956=CARTESIAN_POINT ( 'NONE',  ( -73.52287095715010423, -23.94994826722564696, -0.6494450866342716955 ) ) ;
#88957=CARTESIAN_POINT ( 'NONE',  ( 10.26108024787556516, -17.11367029881254709, -1.500000000000002220 ) ) ;
#88958=EDGE_CURVE ( 'NONE', #82876, #60813, #43654, .T. ) ;
#88960=CARTESIAN_POINT ( 'NONE',  ( 12.81631318294326505, -15.22695477405695996, -1.500000000000002220 ) ) ;
#88961=ORIENTED_EDGE ( 'NONE', *, *, #84601, .T. ) ;
#88962=VECTOR ( 'NONE', #31161, 1000.000000000000114 ) ;
#88963=CARTESIAN_POINT ( 'NONE',  ( -93.62287095715005592, -29.50250786944525672, 11.44777988621623344 ) ) ;
#88968=CARTESIAN_POINT ( 'NONE',  ( -14.80784184970232431, -14.63167926507950689, 11.49999999999999645 ) ) ;
#88971=EDGE_CURVE ( 'NONE', #69148, #90732, #35017, .T. ) ;
#88972=CARTESIAN_POINT ( 'NONE',  ( -51.29687923781917647, -25.26364009307625125, 3.993462176398971497 ) ) ;
#88973=B_SPLINE_CURVE_WITH_KNOTS ( 'NONE', 3,
 ( #54845, #38605, #542, #47227, #69565, #43, #77654, #30989, #85786, #39605, #8663, #93892 ),
 .UNSPECIFIED., .F., .F.,
 ( 4, 2, 2, 2, 2, 4 ),
 ( 0.000000000000000000, 0.0003366851721765631335, 0.0006733703443531262670, 0.001010055516529689400, 0.001178398102617971618, 0.001346740688706254052 ),
 .UNSPECIFIED. ) ;
#88976=CARTESIAN_POINT ( 'NONE',  ( -127.6240570866291080, -24.15543982623907837, -0.2315651400026538520 ) ) ;
#88977=ORIENTED_EDGE ( 'NONE', *, *, #56102, .F. ) ;
#88978=VECTOR ( 'NONE', #53677, 1000.000000000000114 ) ;
#88979=CARTESIAN_POINT ( 'NONE',  ( 18.82617747125253871, -7.458514806974097411, 11.49999999999998934 ) ) ;
#88981=DIRECTION ( 'NONE',  ( 3.773278334444166432E-23, -1.000000000000000000, 0.000000000000000000 ) ) ;
#88984=LINE ( 'NONE', #73261, #61433 ) ;
#88986=CARTESIAN_POINT ( 'NONE',  ( -16.95507112718987486, -10.73317591066004084, -1.500000000000002220 ) ) ;
#88987=CARTESIAN_POINT ( 'NONE',  ( -7.324709186033012465, -19.69651249574825513, 11.49999999999999645 ) ) ;
#88990=CARTESIAN_POINT ( 'NONE',  ( -4.445301477617020325, 21.63612927058290936, 11.49999999999998934 ) ) ;
#88991=CARTESIAN_POINT ( 'NONE',  ( -39.71177198204633640, -25.27806050189757059, 4.822383089495585473 ) ) ;
#88998=ORIENTED_EDGE ( 'NONE', *, *, #15628, .F. ) ;
#88999=CARTESIAN_POINT ( 'NONE',  ( -41.55620429048340014, -23.48786465467240347, 11.44779295918254824 ) ) ;
#89000=CARTESIAN_POINT ( 'NONE',  ( -72.55620429048340725, -23.48786465467240703, 11.44779295918254647 ) ) ;
#89002=CARTESIAN_POINT ( 'NONE',  ( 20.46650637700042097, -2.330123182410055893, -1.500000000000002220 ) ) ;
#89003=CARTESIAN_POINT ( 'NONE',  ( 15.50980990363467882, 14.95361599516425244, 11.49999999999999645 ) ) ;
#89004=VERTEX_POINT ( 'NONE', #55335 ) ;
#89008=CARTESIAN_POINT ( 'NONE',  ( 7.190675130926929448, -21.12231643677837312, -1.500000000000002220 ) ) ;
#89009=B_SPLINE_CURVE_WITH_KNOTS ( 'NONE', 3,
 ( #31668, #62638, #93557, #70741, #81850, #4732 ),
 .UNSPECIFIED., .F., .F.,
 ( 4, 2, 4 ),
 ( 0.000000000000000000, 0.001380764517853252720, 0.002761529035706505441 ),
 .UNSPECIFIED. ) ;
#89010=CARTESIAN_POINT ( 'NONE',  ( -59.62287095715004881, -24.66019654487199020, 8.947790411086131712 ) ) ;
#89011=CARTESIAN_POINT ( 'NONE',  ( -52.62287095715005592, -29.50248528299804818, 1.056150453629033370 ) ) ;
#89012=ORIENTED_EDGE ( 'NONE', *, *, #57798, .T. ) ;
#89013=DIRECTION ( 'NONE',  ( 0.000000000000000000, -0.9999999999976377785, -2.173523156925979975E-06 ) ) ;
#89014=CARTESIAN_POINT ( 'NONE',  ( -83.62287095715007013, -24.65952944569304606, 1.056160979905700792 ) ) ;
#89015=CARTESIAN_POINT ( 'NONE',  ( 16.20321855003292555, -13.12800272717607619, -1.500000000000002220 ) ) ;
#89016=ORIENTED_EDGE ( 'NONE', *, *, #30425, .F. ) ;
#89021=CARTESIAN_POINT ( 'NONE',  ( -51.23552013759741897, -25.28256784800020895, 4.253308875550592560 ) ) ;
#89022=CARTESIAN_POINT ( 'NONE',  ( -6.845587600281468177, 19.88882266644084496, -1.500000000000002220 ) ) ;
#89025=CARTESIAN_POINT ( 'NONE',  ( -114.5895376238167245, -23.48783264082478794, -1.443836473390060382 ) ) ;
#89027=CARTESIAN_POINT ( 'NONE',  ( -120.5901044843091938, -24.40133493613049964, 9.663955038902800609 ) ) ;
#89029=CARTESIAN_POINT ( 'NONE',  ( -81.11504936654542064, -25.25841645967507887, 3.692618488369098895 ) ) ;
#89030=CARTESIAN_POINT ( 'NONE',  ( -49.75955460286667176, -25.13461921803880728, 2.970022368781424671 ) ) ;
#89031=CARTESIAN_POINT ( 'NONE',  ( -13.51661872714272405, -17.00040112538478709, -1.500000000000002220 ) ) ;
#89032=CARTESIAN_POINT ( 'NONE',  ( -81.47155790579010670, -25.24759638701540254, 6.336855562226338279 ) ) ;
#89033=CARTESIAN_POINT ( 'NONE',  ( 19.22371909900314435, 11.20011194808016342, 11.49999999999999645 ) ) ;
#89034=VERTEX_POINT ( 'NONE', #41107 ) ;
#89039=CARTESIAN_POINT ( 'NONE',  ( -35.92287095715006018, -23.47596703998600276, 11.44779298504227683 ) ) ;
#89040=ORIENTED_EDGE ( 'NONE', *, *, #81373, .T. ) ;
#89042=ORIENTED_EDGE ( 'NONE', *, *, #34067, .T. ) ;
#89043=CARTESIAN_POINT ( 'NONE',  ( -75.52287095715007581, -24.63287334234179227, 0.9662140553045428515 ) ) ;
#89045=EDGE_CURVE ( 'NONE', #20987, #92149, #49588, .T. ) ;
#89046=CARTESIAN_POINT ( 'NONE',  ( -43.62287095715006302, -24.50321055353804311, 9.387540953477532923 ) ) ;
#89050=CARTESIAN_POINT ( 'NONE',  ( -83.92287095715009571, -23.47596703998600631, 11.44779298504227860 ) ) ;
#89051=ORIENTED_EDGE ( 'NONE', *, *, #89279, .F. ) ;
#89052=CARTESIAN_POINT ( 'NONE',  ( -130.5728709571500588, -24.33102551592700991, -0.06126342234013575083 ) ) ;
#89053=CARTESIAN_POINT ( 'NONE',  ( -22.33494257564923302, 2.542849975942539587, -1.500000000000002220 ) ) ;
#89054=ORIENTED_EDGE ( 'NONE', *, *, #89465, .T. ) ;
#89055=PLANE ( 'NONE',  #67678 ) ;
#89056=CARTESIAN_POINT ( 'NONE',  ( -94.63996189396370085, -23.48786465467241413, 11.44779295918254469 ) ) ;
#89059=CARTESIAN_POINT ( 'NONE',  ( -63.92295340422755601, -24.66513809378596278, 8.909134979017297340 ) ) ;
#89060=CARTESIAN_POINT ( 'NONE',  ( -9.247272915838292917, -17.29429475886123768, -1.500000000000002220 ) ) ;
#89062=ORIENTED_EDGE ( 'NONE', *, *, #79840, .F. ) ;
#89063=CARTESIAN_POINT ( 'NONE',  ( -20.49900048275977227, -6.559984590058941301, -1.500000000000002220 ) ) ;
#89065=CARTESIAN_POINT ( 'NONE',  ( -42.52287095715005449, -24.66019654487199020, 8.947790411086133489 ) ) ;
#89066=CARTESIAN_POINT ( 'NONE',  ( -101.7776484685884100, -25.27307239909451653, 3.986250617436227550 ) ) ;
#89067=CARTESIAN_POINT ( 'NONE',  ( -70.62287095715005592, -29.50248789122583659, 2.256150453626215580 ) ) ;
#89068=CARTESIAN_POINT ( 'NONE',  ( -16.20615075098634961, 16.30094363606528418, -1.500000000000002220 ) ) ;
#89072=CARTESIAN_POINT ( 'NONE',  ( -19.96166555454951208, -2.086822695551191043, 11.49999999999999645 ) ) ;
#89073=CARTESIAN_POINT ( 'NONE',  ( -68.52287095715006160, -23.47596703998600631, 11.44779298504228748 ) ) ;
#89077=CARTESIAN_POINT ( 'NONE',  ( -82.52287095715003318, -24.33927499327855770, 9.819080762295817166 ) ) ;
#89078=CARTESIAN_POINT ( 'NONE',  ( -1.214729172165279092, -19.82145330704504360, -1.500000000000002220 ) ) ;
#89080=CARTESIAN_POINT ( 'NONE',  ( -113.6281192877314368, -23.96119346886881374, -0.6495511937832029181 ) ) ;
#89081=CARTESIAN_POINT ( 'NONE',  ( -0.8432318219891272726, -19.69000482574202238, -1.500000000000002220 ) ) ;
#89082=CARTESIAN_POINT ( 'NONE',  ( -91.94687923781918926, -25.23397913219354649, 6.409327625488847602 ) ) ;
#89084=EDGE_CURVE ( 'NONE', #39801, #62532, #90720, .T. ) ;
#89085=CARTESIAN_POINT ( 'NONE',  ( -123.5228709571500616, -24.64965694238408034, 8.947790433994191162 ) ) ;
#89086=PLANE ( 'NONE',  #23218 ) ;
#89087=CARTESIAN_POINT ( 'NONE',  ( 0.06016934085327452914, 20.63536315578604174, 11.49999999999999645 ) ) ;
#89090=CARTESIAN_POINT ( 'NONE',  ( -33.52287095715006160, -23.47596703998600631, 11.44779298504229459 ) ) ;
#89091=CARTESIAN_POINT ( 'NONE',  ( 14.05383982582471170, -17.77673030755399708, 11.49999999999999645 ) ) ;
#89093=DIRECTION ( 'NONE',  ( 3.773278334444166432E-23, -1.000000000000000000, 0.000000000000000000 ) ) ;
#89094=CARTESIAN_POINT ( 'NONE',  ( -39.52287095715006870, -29.50250243563736774, 8.947779886222148704 ) ) ;
#89097=CARTESIAN_POINT ( 'NONE',  ( -127.5228709571500616, -24.64965694238408034, 8.947790433994189385 ) ) ;
#89100=ORIENTED_EDGE ( 'NONE', *, *, #3857, .T. ) ;
#89101=B_SPLINE_CURVE_WITH_KNOTS ( 'NONE', 3,
 ( #1281, #56576, #24595, #86004 ),
 .UNSPECIFIED., .F., .F.,
 ( 4, 4 ),
 ( 0.000000000000000000, 9.999999999998897304E-05 ),
 .UNSPECIFIED. ) ;
#89102=EDGE_LOOP ( 'NONE', ( #98786, #18104, #26803, #59097 ) ) ;
#89104=CARTESIAN_POINT ( 'NONE',  ( -11.09240565882118368, -20.00103931635436538, 11.49999999999998934 ) ) ;
#89107=CARTESIAN_POINT ( 'NONE',  ( -18.50814150397365410, 11.09706937414969374, -1.500000000000002220 ) ) ;
#89109=PLANE ( 'NONE',  #35505 ) ;
#89110=CARTESIAN_POINT ( 'NONE',  ( 22.42242567092132433, 2.420433022335332751, 11.49999999999999645 ) ) ;
#89111=VERTEX_POINT ( 'NONE', #19739 ) ;
#89112=VECTOR ( 'NONE', #12345, 1000.000000000000114 ) ;
#89114=CARTESIAN_POINT ( 'NONE',  ( 20.57779966680088890, -7.652443150423321683, 11.49999999999998934 ) ) ;
#89117=DIRECTION ( 'NONE',  ( -3.773278334453079030E-23, 0.9999999999976377785, 2.173523156925979128E-06 ) ) ;
#89119=CARTESIAN_POINT ( 'NONE',  ( -112.6228709571500559, -29.50250243563736774, 8.947779886222136270 ) ) ;
#89120=CARTESIAN_POINT ( 'NONE',  ( -47.58953762381673158, -23.47596703998600276, 11.44779298504227505 ) ) ;
#89121=VERTEX_POINT ( 'NONE', #74539 ) ;
#89122=CARTESIAN_POINT ( 'NONE',  ( -77.62287095715005592, -23.47593901973091235, -1.443836447539004642 ) ) ;
#89123=EDGE_LOOP ( 'NONE', ( #60667, #48713, #24253, #85229 ) ) ;
#89125=ORIENTED_EDGE ( 'NONE', *, *, #60213, .T. ) ;
#89126=CARTESIAN_POINT ( 'NONE',  ( -126.5228709571500616, -23.47593901973090524, -1.443836447538996204 ) ) ;
#89128=FACE_OUTER_BOUND ( 'NONE', #39186, .T. ) ;
#89129=CARTESIAN_POINT ( 'NONE',  ( 19.36038471569032993, -6.267470172042458820, -1.500000000000002220 ) ) ;
#89131=CARTESIAN_POINT ( 'NONE',  ( -70.70154144008259323, -25.04161745251516180, 7.522173495007288047 ) ) ;
#89132=CARTESIAN_POINT ( 'NONE',  ( -29.64366785207624488, -24.08068896706512163, 10.23563548314527338 ) ) ;
#89133=ADVANCED_FACE ( 'NONE', ( #75524 ), #29917, .T. ) ;
#89134=CARTESIAN_POINT ( 'NONE',  ( -89.40841769935767047, -25.11033443737731474, 2.832404817301930056 ) ) ;
#89135=CARTESIAN_POINT ( 'NONE',  ( -71.43409008949743111, -25.03149735735439307, 7.038381313596293154 ) ) ;
#89137=CARTESIAN_POINT ( 'NONE',  ( -28.29914910988898669, -24.76880887354685612, 2.427551041383773978 ) ) ;
#89138=B_SPLINE_CURVE_WITH_KNOTS ( 'NONE', 3,
 ( #17630, #33347, #80029, #49597, #81539, #35366 ),
 .UNSPECIFIED., .F., .F.,
 ( 4, 2, 4 ),
 ( 6.391158118969316353E-06, 0.001387004593080787881, 0.002767618028042606766 ),
 .UNSPECIFIED. ) ;
#89139=DIRECTION ( 'NONE',  ( 3.773278334444166432E-23, -1.000000000000000000, 0.000000000000000000 ) ) ;
#89141=CARTESIAN_POINT ( 'NONE',  ( 1.212613378922696050, -20.72488358683818888, -1.500000000000002220 ) ) ;
#89142=ORIENTED_EDGE ( 'NONE', *, *, #92375, .F. ) ;
#89144=FACE_OUTER_BOUND ( 'NONE', #57704, .T. ) ;
#89145=EDGE_LOOP ( 'NONE', ( #21772, #89467, #16855, #93841 ) ) ;
#89146=CARTESIAN_POINT ( 'NONE',  ( -86.62287095715004170, -24.51283580621364067, 0.6167428607019888043 ) ) ;
#89148=VERTEX_POINT ( 'NONE', #12637 ) ;
#89149=ORIENTED_EDGE ( 'NONE', *, *, #15234, .F. ) ;
#89152=CARTESIAN_POINT ( 'NONE',  ( -52.62287095715005592, -23.48786465467240703, 11.44779295918255002 ) ) ;
#89153=CARTESIAN_POINT ( 'NONE',  ( -43.61624872165830880, -23.48786465467240347, 11.44779295918255180 ) ) ;
#89154=CARTESIAN_POINT ( 'NONE',  ( 18.22792733936863030, -12.41963300964812156, 11.49999999999999645 ) ) ;
#89155=ORIENTED_EDGE ( 'NONE', *, *, #84338, .F. ) ;
#89156=CARTESIAN_POINT ( 'NONE',  ( -108.6294904440730136, -23.96119346886881374, -0.6495511937831862648 ) ) ;
#89157=CARTESIAN_POINT ( 'NONE',  ( 19.70651319644445465, -11.07993823016455792, 11.49999999999998934 ) ) ;
#89158=CARTESIAN_POINT ( 'NONE',  ( -115.5516328901577197, -24.73531770709096023, 8.716586749053508498 ) ) ;
#89159=ORIENTED_EDGE ( 'NONE', *, *, #98689, .T. ) ;
#89164=B_SPLINE_CURVE_WITH_KNOTS ( 'NONE', 3,
 ( #18883, #80290, #87908, #72688, #19875, #19383, #80796, #81789 ),
 .UNSPECIFIED., .F., .F.,
 ( 4, 2, 2, 4 ),
 ( 0.000000000000000000, 0.002001098010032688421, 0.003001647015049031114, 0.004002196020065373373 ),
 .UNSPECIFIED. ) ;
#89165=CARTESIAN_POINT ( 'NONE',  ( -57.58282881803972231, -24.51419770103157347, 9.386484678747176957 ) ) ;
#89167=CARTESIAN_POINT ( 'NONE',  ( 12.09327641706010326, 17.40255341615222306, -1.500000000000002220 ) ) ;
#89170=CARTESIAN_POINT ( 'NONE',  ( -41.86766821746776657, -25.28562906917319353, 4.300397852270189780 ) ) ;
#89171=CARTESIAN_POINT ( 'NONE',  ( -13.70410651198969809, -17.55484038775568933, -1.500000000000002220 ) ) ;
#89173=B_SPLINE_CURVE_WITH_KNOTS ( 'NONE', 3,
 ( #1486, #79085, #77579, #32425, #62897, #63397, #8589, #33417, #39033, #1986, #71499, #39538, #9587, #79594, #69982, #94818 ),
 .UNSPECIFIED., .F., .F.,
 ( 4, 2, 2, 2, 2, 2, 2, 4 ),
 ( 0.000000000000000000, 0.0003118384806944565074, 0.0006236769613889130148, 0.001247353922777823428, 0.001559192403472278851, 0.001871030884166734057, 0.002182869364861189480, 0.002494707845555644687 ),
 .UNSPECIFIED. ) ;
#89175=CARTESIAN_POINT ( 'NONE',  ( -54.52287095715006870, -24.65952944569304606, 1.056160979905693686 ) ) ;
#89177=EDGE_CURVE ( 'NONE', #17220, #77901, #8411, .T. ) ;
#89180=VECTOR ( 'NONE', #50115, 1000.000000000000114 ) ;
#89181=CARTESIAN_POINT ( 'NONE',  ( -17.64752530894654470, 8.349842952099315596, -1.500000000000002220 ) ) ;
#89183=CARTESIAN_POINT ( 'NONE',  ( 18.29419249859179786, 11.19154738541161365, 11.49999999999998934 ) ) ;
#89184=CARTESIAN_POINT ( 'NONE',  ( -27.40838375831408058, -24.92774670570336326, 1.648156544774445731 ) ) ;
#89185=B_SPLINE_CURVE_WITH_KNOTS ( 'NONE', 3,
 ( #38434, #45561, #21199, #83599, #37441, #99807 ),
 .UNSPECIFIED., .F., .F.,
 ( 4, 2, 4 ),
 ( 1.570755371633875854E-05, 0.001396183895866086452, 0.002776660238015833844 ),
 .UNSPECIFIED. ) ;
#89187=CARTESIAN_POINT ( 'NONE',  ( -77.52212617553594498, -23.48783264082476663, -1.443836473390097241 ) ) ;
#89188=CARTESIAN_POINT ( 'NONE',  ( -22.76716317511769461, -1.676022972194794791, -1.500000000000002220 ) ) ;
#89193=CARTESIAN_POINT ( 'NONE',  ( 19.80199147212610811, 2.383747631481649254, 11.49999999999999645 ) ) ;
#89194=CARTESIAN_POINT ( 'NONE',  ( -31.52287095715006160, -24.64898659630367206, 1.056161002820817485 ) ) ;
#89196=CARTESIAN_POINT ( 'NONE',  ( -48.48463779374034743, -24.65952944569304606, 1.056160979905697461 ) ) ;
#89197=EDGE_CURVE ( 'NONE', #62610, #38959, #48308, .T. ) ;
#89198=ORIENTED_EDGE ( 'NONE', *, *, #47058, .T. ) ;
#89199=DIRECTION ( 'NONE',  ( 0.000000000000000000, 0.9999999999976377785, 2.173523156925979975E-06 ) ) ;
#89200=CARTESIAN_POINT ( 'NONE',  ( -33.00286163603178125, -25.16202561908117730, 2.791798636425737445 ) ) ;
#89201=CARTESIAN_POINT ( 'NONE',  ( 21.21565077533257337, 4.556159429511043690, 11.49999999999998934 ) ) ;
#89202=CARTESIAN_POINT ( 'NONE',  ( -84.52287095715010423, -24.35013146730203815, 9.818937971375104823 ) ) ;
#89203=CARTESIAN_POINT ( 'NONE',  ( 19.26631176993168282, 3.279242639417544236, -1.500000000000002220 ) ) ;
#89204=LINE ( 'NONE', #80088, #39336 ) ;
#89205=B_SPLINE_CURVE_WITH_KNOTS ( 'NONE', 3,
 ( #49293, #19311, #17824, #80726, #58399, #48280 ),
 .UNSPECIFIED., .F., .F.,
 ( 4, 2, 4 ),
 ( 0.000000000000000000, 0.001380901958385389195, 0.002761803916770778390 ),
 .UNSPECIFIED. ) ;
#89207=ADVANCED_FACE ( 'NONE', ( #73550 ), #4042, .F. ) ;
#89208=CARTESIAN_POINT ( 'NONE',  ( -51.58953762381672448, -24.66019654487199020, 8.947790411086131712 ) ) ;
#89209=CARTESIAN_POINT ( 'NONE',  ( -18.16121111207539940, 9.348575961806686152, 11.49999999999999645 ) ) ;
#89210=CARTESIAN_POINT ( 'NONE',  ( -50.31093898778911466, -25.30399390996193532, 5.199283961936068899 ) ) ;
#89211=EDGE_CURVE ( 'NONE', #61226, #74791, #81027, .T. ) ;
#89212=CARTESIAN_POINT ( 'NONE',  ( -89.52287095715007581, -24.50216790748204687, 0.6166512839542543922 ) ) ;
#89215=CARTESIAN_POINT ( 'NONE',  ( -49.21454750704995007, -29.50249835244419927, 7.069174116995804447 ) ) ;
#89217=EDGE_CURVE ( 'NONE', #99833, #89034, #9398, .T. ) ;
#89218=CARTESIAN_POINT ( 'NONE',  ( -56.22287095715006444, -23.47593901973090169, -1.443836447538997536 ) ) ;
#89221=CARTESIAN_POINT ( 'NONE',  ( 22.99805582222048272, -0.5679727363130141482, 11.49999999999999645 ) ) ;
#89222=CARTESIAN_POINT ( 'NONE',  ( -22.77908990650604792, -0.06651829912971220227, 11.49999999999998934 ) ) ;
#89224=CARTESIAN_POINT ( 'NONE',  ( -40.52287095715005449, -24.99132157543166244, 2.256160258750667502 ) ) ;
#89226=CARTESIAN_POINT ( 'NONE',  ( -70.52287095715007581, -23.48783264082477018, -1.443836473390089914 ) ) ;
#89227=CARTESIAN_POINT ( 'NONE',  ( -110.5598941975710119, -23.48783264082476308, -1.443836473390091468 ) ) ;
#89229=CARTESIAN_POINT ( 'NONE',  ( 1.740910633133015972, 21.82039641801506846, -1.500000000000002220 ) ) ;
#89231=DIRECTION ( 'NONE',  ( -3.773278334453080206E-23, 0.9999999999976377785, 2.173523156925979975E-06 ) ) ;
#89232=FACE_OUTER_BOUND ( 'NONE', #66645, .T. ) ;
#89234=ORIENTED_EDGE ( 'NONE', *, *, #83229, .T. ) ;
#89235=CARTESIAN_POINT ( 'NONE',  ( -4.163110563111144913, -19.98234244090558320, -1.500000000000002220 ) ) ;
#89240=CARTESIAN_POINT ( 'NONE',  ( 22.99805582222048272, -0.5679727363130141482, -1.500000000000002220 ) ) ;
#89241=LINE ( 'NONE', #74506, #19489 ) ;
#89242=CARTESIAN_POINT ( 'NONE',  ( 13.23653054071972512, 15.24542462990338088, -1.500000000000002220 ) ) ;
#89243=ORIENTED_EDGE ( 'NONE', *, *, #3775, .T. ) ;
#89244=CARTESIAN_POINT ( 'NONE',  ( -113.5228709571501327, -24.66019654487200441, 8.947790411086112172 ) ) ;
#89247=CARTESIAN_POINT ( 'NONE',  ( -73.62287095715005592, -29.50248528299804818, 1.056150453629036701 ) ) ;
#89249=CARTESIAN_POINT ( 'NONE',  ( 20.90283063341239966, -4.354886778353011856, 11.49999999999999645 ) ) ;
#89250=ORIENTED_EDGE ( 'NONE', *, *, #85761, .F. ) ;
#89252=AXIS2_PLACEMENT_3D ( 'NONE', #11372, #25086, #64694 ) ;
#89253=EDGE_LOOP ( 'NONE', ( #13491, #47983, #48255, #33773 ) ) ;
#89254=CARTESIAN_POINT ( 'NONE',  ( 7.309977242446557888, -21.02818303981469583, -1.500000000000002220 ) ) ;
#89255=CARTESIAN_POINT ( 'NONE',  ( 9.361532043782798240, 18.45020211870636118, 11.49999999999998934 ) ) ;
#89258=LINE ( 'NONE', #88261, #46953 ) ;
#89259=ORIENTED_EDGE ( 'NONE', *, *, #76160, .T. ) ;
#89263=CARTESIAN_POINT ( 'NONE',  ( -16.13976855045889636, 13.32451261336467496, -1.500000000000002220 ) ) ;
#89264=CARTESIAN_POINT ( 'NONE',  ( -8.129759772327192380, 20.32010563749377141, 11.49999999999999645 ) ) ;
#89265=CARTESIAN_POINT ( 'NONE',  ( -26.33488822642538452, -24.77993562733889732, 6.524122098704422612 ) ) ;
#89266=CARTESIAN_POINT ( 'NONE',  ( -21.16606679798846358, 7.723709098063864076, -1.500000000000002220 ) ) ;
#89267=CARTESIAN_POINT ( 'NONE',  ( 20.69369447470243628, -3.267675865747468489, 11.49999999999998934 ) ) ;
#89268=DIRECTION ( 'NONE',  ( -3.773278334453080206E-23, 0.9999999999976377785, 2.173523156925979552E-06 ) ) ;
#89270=CARTESIAN_POINT ( 'NONE',  ( -29.62287095715004881, -24.58457514626677209, 8.947790440257529454 ) ) ;
#89273=EDGE_LOOP ( 'NONE', ( #48820, #46683, #13558, #67996 ) ) ;
#89275=B_SPLINE_CURVE_WITH_KNOTS ( 'NONE', 3,
 ( #21867, #43737, #44733, #74670, #36118, #90899, #20879, #82783, #13265, #36611 ),
 .UNSPECIFIED., .F., .F.,
 ( 4, 3, 3, 4 ),
 ( 3.074392035520069841E-15, 0.0001187729392939394833, 0.0002375726806888468626, 0.0004748969025384985692 ),
 .UNSPECIFIED. ) ;
#89276=B_SPLINE_CURVE_WITH_KNOTS ( 'NONE', 3,
 ( #70105, #53886, #94436, #55900 ),
 .UNSPECIFIED., .F., .F.,
 ( 4, 4 ),
 ( 0.9304503362875529149, 0.9394567675596684486 ),
 .UNSPECIFIED. ) ;
#89277=CARTESIAN_POINT ( 'NONE',  ( -99.31542661674430406, -25.12215508542761810, 6.334584756663662830 ) ) ;
#89278=VERTEX_POINT ( 'NONE', #31237 ) ;
#89279=EDGE_CURVE ( 'NONE', #733, #77757, #78901, .T. ) ;
#89280=CARTESIAN_POINT ( 'NONE',  ( 12.90647603486358364, 17.18646895862681134, -1.500000000000002220 ) ) ;
#89281=CARTESIAN_POINT ( 'NONE',  ( -95.62287095715005592, -23.47593901973091235, -1.443836447539001089 ) ) ;
#89283=CARTESIAN_POINT ( 'NONE',  ( 14.35337761433406811, 15.45585641580067104, 11.49999999999998934 ) ) ;
#89285=CARTESIAN_POINT ( 'NONE',  ( -52.62287095715009144, -24.34917612406838217, 0.1852690917426617345 ) ) ;
#89286=EDGE_CURVE ( 'NONE', #81354, #97718, #20428, .T. ) ;
#89287=FACE_OUTER_BOUND ( 'NONE', #88403, .T. ) ;
#89288=CARTESIAN_POINT ( 'NONE',  ( -101.6270331350176548, -24.34968618360934300, 0.1864209137778871650 ) ) ;
#89290=CARTESIAN_POINT ( 'NONE',  ( 15.76968270297436625, 15.47746201419723100, -1.500000000000002220 ) ) ;
#89292=CARTESIAN_POINT ( 'NONE',  ( -81.59191989886164720, -24.15620529776628445, 10.23563542870661180 ) ) ;
#89294=CARTESIAN_POINT ( 'NONE',  ( -41.81544514806834201, -25.31624538345576170, 4.607988139056270249 ) ) ;
#89295=EDGE_CURVE ( 'NONE', #69268, #74882, #88217, .T. ) ;
#89297=CARTESIAN_POINT ( 'NONE',  ( -47.52287095715006160, -24.50216790748205042, 0.6166512839542448443 ) ) ;
#89300=CARTESIAN_POINT ( 'NONE',  ( 12.49974722350246736, 17.29906535522423638, -1.500000000000002220 ) ) ;
#89301=CARTESIAN_POINT ( 'NONE',  ( -26.11716922332098534, -24.96254238629463984, 5.477951238729472649 ) ) ;
#89302=CARTESIAN_POINT ( 'NONE',  ( -49.89395067847572562, -25.03707831087709579, 7.590867751134624974 ) ) ;
#89304=CARTESIAN_POINT ( 'NONE',  ( -64.63157754250315179, -24.35071581493543391, 9.817618358456023486 ) ) ;
#89305=DIRECTION ( 'NONE',  ( 0.000000000000000000, 0.9999999999976377785, 2.173523156925979128E-06 ) ) ;
#89306=CARTESIAN_POINT ( 'NONE',  ( -4.753580043990282888, 22.13494492317406070, -1.500000000000002220 ) ) ;
#89307=CARTESIAN_POINT ( 'NONE',  ( -33.52287095715006160, -23.47596703998600631, 11.44779298504229459 ) ) ;
#89309=CARTESIAN_POINT ( 'NONE',  ( -50.72885261542558055, -25.31331831088759188, 5.238457455606527091 ) ) ;
#89310=PLANE ( 'NONE',  #78357 ) ;
#89311=CARTESIAN_POINT ( 'NONE',  ( -8.281543130087330340, -17.94227898472161797, 11.49999999999999645 ) ) ;
#89312=CARTESIAN_POINT ( 'NONE',  ( -82.62287095715004170, -23.47596703998600631, 11.44779298504227860 ) ) ;
#89317=CARTESIAN_POINT ( 'NONE',  ( -70.52287095715009002, -24.15516710230294350, 10.28746687063725673 ) ) ;
#89319=CARTESIAN_POINT ( 'NONE',  ( -13.25059585359799108, -17.08168364658555305, 11.49999999999998934 ) ) ;
#89321=CARTESIAN_POINT ( 'NONE',  ( -13.43510958081001050, -13.94331287200543024, -1.500000000000002220 ) ) ;
#89322=DIRECTION ( 'NONE',  ( -3.773278334444167608E-23, 1.000000000000000000, 0.000000000000000000 ) ) ;
#89323=LINE ( 'NONE', #95932, #37744 ) ;
#89324=CARTESIAN_POINT ( 'NONE',  ( -13.31955177964949755, -14.60123061082138385, -1.500000000000002220 ) ) ;
#89328=CARTESIAN_POINT ( 'NONE',  ( -9.609455416251792670, -17.83980533922896683, 11.49999999999999645 ) ) ;
#89329=CARTESIAN_POINT ( 'NONE',  ( -54.55620429048340014, -24.66019654487198309, 8.947790411086135265 ) ) ;
#89330=EDGE_CURVE ( 'NONE', #7606, #16795, #83645, .T. ) ;
#89331=CARTESIAN_POINT ( 'NONE',  ( -44.52287095715007581, -24.34917612406836795, 0.1852690917426490502 ) ) ;
#89332=ADVANCED_FACE ( 'NONE', ( #38849 ), #55092, .F. ) ;
#89335=LINE ( 'NONE', #5588, #41251 ) ;
#89336=CARTESIAN_POINT ( 'NONE',  ( -44.62287095715004881, -24.65952944569303895, 1.056160979905693686 ) ) ;
#89337=CARTESIAN_POINT ( 'NONE',  ( -32.52287095715006160, -24.64965694238575011, 8.947790433994207149 ) ) ;
#89338=CARTESIAN_POINT ( 'NONE',  ( -86.62287095715001328, -23.47596703998600631, 11.44779298504227683 ) ) ;
#89339=CARTESIAN_POINT ( 'NONE',  ( 20.02521558760690112, -0.9251608499524575091, -1.500000000000002220 ) ) ;
#89340=B_SPLINE_CURVE_WITH_KNOTS ( 'NONE', 3,
 ( #68002, #35557, #44161, #75093, #98932, #27933, #29420, #60402, #91323, #76090, #37543, #68493, #12195, #58890, #21796, #58400 ),
 .UNSPECIFIED., .F., .F.,
 ( 4, 2, 2, 2, 2, 2, 2, 4 ),
 ( 8.673617379884035472E-19, 0.0002012182839424428243, 0.0004024365678848847811, 0.0006036548518273267923, 0.0008048731357697686949, 0.001207309703654670281, 0.001408527987597120749, 0.001609746271539571651 ),
 .UNSPECIFIED. ) ;
#89343=ORIENTED_EDGE ( 'NONE', *, *, #58045, .T. ) ;
#89344=EDGE_CURVE ( 'NONE', #17471, #7644, #60369, .T. ) ;
#89345=EDGE_CURVE ( 'NONE', #72609, #99097, #8903, .T. ) ;
#89346=CARTESIAN_POINT ( 'NONE',  ( -103.5228709571501184, -23.96177878511309345, 10.65340807706329507 ) ) ;
#89347=CARTESIAN_POINT ( 'NONE',  ( -29.62287095715004881, -24.58457514626677209, 8.947790440257529454 ) ) ;
#89348=CARTESIAN_POINT ( 'NONE',  ( -79.56153920765868293, -25.30148319546968239, 5.323200279246012023 ) ) ;
#89350=CARTESIAN_POINT ( 'NONE',  ( -89.40841769935767047, -25.05712065398430966, 7.447789548358837663 ) ) ;
#89351=CARTESIAN_POINT ( 'NONE',  ( -50.62287095715005592, -29.50247984919015209, -1.443849546365058689 ) ) ;
#89353=CARTESIAN_POINT ( 'NONE',  ( -3.780122020211411193, 19.97858748211865532, 11.49999999999998934 ) ) ;
#89355=CARTESIAN_POINT ( 'NONE',  ( -19.87571804785047647, -11.42512898079034400, -1.500000000000002220 ) ) ;
#89357=ORIENTED_EDGE ( 'NONE', *, *, #3861, .F. ) ;
#89358=DIRECTION ( 'NONE',  ( -1.000000000000000000, -3.773278334444167608E-23, -8.201307833595939069E-29 ) ) ;
#89359=CARTESIAN_POINT ( 'NONE',  ( -49.27764846858840997, -25.26263970634994749, 6.145204967039955335 ) ) ;
#89360=CARTESIAN_POINT ( 'NONE',  ( -72.52287095715007581, -23.47593901973090169, -1.443836447538996870 ) ) ;
#89361=CARTESIAN_POINT ( 'NONE',  ( 18.56724428474754518, 10.22298014144217859, 11.49999999999999645 ) ) ;
#89362=CARTESIAN_POINT ( 'NONE',  ( 2.574831182292884435, -22.01391258260016315, 11.49999999999998934 ) ) ;
#89364=CARTESIAN_POINT ( 'NONE',  ( 11.80677006232881254, 16.86875346446678137, 11.49999999999998934 ) ) ;
#89365=EDGE_LOOP ( 'NONE', ( #63953, #64732, #82020, #57035, #95105, #84761 ) ) ;
#89366=PLANE ( 'NONE',  #89577 ) ;
#89368=PLANE ( 'NONE',  #23555 ) ;
#89369=CARTESIAN_POINT ( 'NONE',  ( -50.52287095715007581, -23.84081130425355965, 10.88220057483161263 ) ) ;
#89370=ORIENTED_EDGE ( 'NONE', *, *, #69473, .F. ) ;
#89374=CARTESIAN_POINT ( 'NONE',  ( -83.62287095715005592, -23.48783264082478794, -1.443836473390065711 ) ) ;
#89375=CARTESIAN_POINT ( 'NONE',  ( -126.6228709571500559, -29.50248528299804818, 1.056150453629047137 ) ) ;
#89377=CARTESIAN_POINT ( 'NONE',  ( 17.70469293622815243, 10.90570606759641592, -1.500000000000002220 ) ) ;
#89378=CARTESIAN_POINT ( 'NONE',  ( -3.653784360050144286, 21.42803128968991544, 11.49999999999999645 ) ) ;
#89379=ORIENTED_EDGE ( 'NONE', *, *, #3051, .F. ) ;
#89381=CARTESIAN_POINT ( 'NONE',  ( -119.6228709571501128, -24.51387760970725083, 9.387446482453411178 ) ) ;
#89382=CARTESIAN_POINT ( 'NONE',  ( 18.78116726530667080, 12.29669497462397842, -1.500000000000002220 ) ) ;
#89384=CARTESIAN_POINT ( 'NONE',  ( -65.60613133360229199, -23.85016227208580730, -0.8807180028928343063 ) ) ;
#89386=CARTESIAN_POINT ( 'NONE',  ( -75.52287095715007581, -24.51163499207174823, 0.6490370598554360271 ) ) ;
#89388=CARTESIAN_POINT ( 'NONE',  ( -85.55620429048340725, -24.99132157543166954, 2.256160258750668834 ) ) ;
#89392=CARTESIAN_POINT ( 'NONE',  ( -46.57703336374709124, -24.66019654487199375, 8.947790411086122830 ) ) ;
#89393=ORIENTED_EDGE ( 'NONE', *, *, #49918, .T. ) ;
#89395=CARTESIAN_POINT ( 'NONE',  ( 6.557060941508195739, 20.25493142521265355, -1.500000000000002220 ) ) ;
#89396=ORIENTED_EDGE ( 'NONE', *, *, #39910, .F. ) ;
#89397=CARTESIAN_POINT ( 'NONE',  ( -88.58576889810002797, -24.51314013834316086, 0.6176544820404141767 ) ) ;
#89399=CARTESIAN_POINT ( 'NONE',  ( 21.83365961380331655, 0.8745889840297637052, 11.49999999999998934 ) ) ;
#89401=CARTESIAN_POINT ( 'NONE',  ( 12.08046422559826816, 19.21373320108137861, 11.49999999999998934 ) ) ;
#89404=CARTESIAN_POINT ( 'NONE',  ( -9.857428550561325054, -19.57614489166009264, -1.500000000000002220 ) ) ;
#89407=CARTESIAN_POINT ( 'NONE',  ( -122.5535487218200217, -24.66019654487200086, 8.947790411086110396 ) ) ;
#89408=CARTESIAN_POINT ( 'NONE',  ( -73.58953762381673869, -24.64898659630367916, 1.056161002820384054 ) ) ;
#89410=VERTEX_POINT ( 'NONE', #64728 ) ;
#89412=CARTESIAN_POINT ( 'NONE',  ( -90.62287095715004170, -24.15431212366389957, -0.2830839119429071626 ) ) ;
#89413=ORIENTED_EDGE ( 'NONE', *, *, #12278, .F. ) ;
#89417=CARTESIAN_POINT ( 'NONE',  ( 1.567330217057175901, -21.20382687294985047, -1.500000000000002220 ) ) ;
#89418=CARTESIAN_POINT ( 'NONE',  ( -98.62536759172499501, -24.51419770103156992, 9.386484678747175181 ) ) ;
#89420=CARTESIAN_POINT ( 'NONE',  ( -85.50202734187257647, -24.63355581998384736, 0.9682620441943965428 ) ) ;
#89423=B_SPLINE_CURVE_WITH_KNOTS ( 'NONE', 3,
 ( #50156, #26313, #88220, #80094, #81094, #10578 ),
 .UNSPECIFIED., .F., .F.,
 ( 4, 2, 4 ),
 ( 1.570755371634415583E-05, 0.001396183895866092740, 0.002776660238015841217 ),
 .UNSPECIFIED. ) ;
#89424=CARTESIAN_POINT ( 'NONE',  ( -44.62287095715005592, -24.50321055353805733, 9.387540953477532923 ) ) ;
#89425=EDGE_LOOP ( 'NONE', ( #4692, #69603, #73673, #31462 ) ) ;
#89426=CARTESIAN_POINT ( 'NONE',  ( -18.73025074496528219, 5.678645368852136777, 11.49999999999999645 ) ) ;
#89427=CARTESIAN_POINT ( 'NONE',  ( -99.21417444527331497, -25.30351579687176411, 4.454760979438658453 ) ) ;
#89428=CARTESIAN_POINT ( 'NONE',  ( -29.68470166834870838, -25.15597160735836368, 6.410310830211703781 ) ) ;
#89429=ADVANCED_FACE ( 'NONE', ( #50978 ), #53430, .T. ) ;
#89432=CARTESIAN_POINT ( 'NONE',  ( -40.52287095715006870, -23.47596703998600631, 11.44779298504229281 ) ) ;
#89433=PLANE ( 'NONE',  #32569 ) ;
#89434=CARTESIAN_POINT ( 'NONE',  ( -62.58953762381672448, -23.48783264082478794, -1.443836473390068820 ) ) ;
#89435=CARTESIAN_POINT ( 'NONE',  ( 19.16472379399037251, -4.548241762842377689, 11.49999999999998934 ) ) ;
#89436=EDGE_CURVE ( 'NONE', #40482, #16731, #56779, .T. ) ;
#89437=ORIENTED_EDGE ( 'NONE', *, *, #68747, .T. ) ;
#89438=VECTOR ( 'NONE', #50396, 1000.000000000000114 ) ;
#89439=CARTESIAN_POINT ( 'NONE',  ( -103.5228709571500758, -29.50247984919015209, -1.443849546365050029 ) ) ;
#89441=EDGE_CURVE ( 'NONE', #38032, #59306, #80916, .T. ) ;
#89444=CARTESIAN_POINT ( 'NONE',  ( -74.52287095715007581, -23.48783264082476308, -1.443836473390090802 ) ) ;
#89445=CARTESIAN_POINT ( 'NONE',  ( -59.62287095715007723, -23.47596703998600276, 11.44779298504227683 ) ) ;
#89446=CARTESIAN_POINT ( 'NONE',  ( -47.62369814497165521, -24.65952944569304606, 1.056160979905696129 ) ) ;
#89447=CARTESIAN_POINT ( 'NONE',  ( -118.5174284418064872, -24.51314013834317151, 0.6176544820404247238 ) ) ;
#89449=CARTESIAN_POINT ( 'NONE',  ( -75.92287095715006728, -23.47596703998600631, 11.44779298504227860 ) ) ;
#89450=DIRECTION ( 'NONE',  ( -3.773278334444167608E-23, 1.000000000000000000, 0.000000000000000000 ) ) ;
#89451=CARTESIAN_POINT ( 'NONE',  ( 16.68016870136555596, 10.92824754362290385, -1.500000000000002220 ) ) ;
#89452=CARTESIAN_POINT ( 'NONE',  ( -0.08873648434230119175, -21.90123647746391455, 10.22788351244709482 ) ) ;
#89453=CARTESIAN_POINT ( 'NONE',  ( 19.12242951303546334, 5.485007674754557527, -1.500000000000002220 ) ) ;
#89459=B_SPLINE_CURVE_WITH_KNOTS ( 'NONE', 3,
 ( #84823, #68118, #38651, #100028 ),
 .UNSPECIFIED., .F., .F.,
 ( 4, 4 ),
 ( 0.000000000000000000, 1.000000000000000000 ),
 .UNSPECIFIED. ) ;
#89463=CARTESIAN_POINT ( 'NONE',  ( -49.62287095715005592, -23.48786465467241058, 11.44779295918254824 ) ) ;
#89465=EDGE_CURVE ( 'NONE', #87638, #98717, #84602, .T. ) ;
#89467=ORIENTED_EDGE ( 'NONE', *, *, #95946, .F. ) ;
#89470=VERTEX_POINT ( 'NONE', #42870 ) ;
#89471=CARTESIAN_POINT ( 'NONE',  ( 20.02926185082240451, -2.967945350358753398, 11.49999999999998934 ) ) ;
#89472=CARTESIAN_POINT ( 'NONE',  ( -43.62287095715004881, -23.48783264082477729, -1.443836473390071928 ) ) ;
#89473=DIRECTION ( 'NONE',  ( 0.000000000000000000, -2.173523156925980399E-06, 0.9999999999976378895 ) ) ;
#89474=DIRECTION ( 'NONE',  ( 0.000000000000000000, -2.173523156925980399E-06, 0.9999999999976378895 ) ) ;
#89476=CARTESIAN_POINT ( 'NONE',  ( -79.39668153920749205, -25.31497848055487765, 4.862330694693304700 ) ) ;
#89478=CARTESIAN_POINT ( 'NONE',  ( -5.826506878040391690, 19.21762618028343184, -1.500000000000002220 ) ) ;
#89479=CARTESIAN_POINT ( 'NONE',  ( 20.41947327098772647, -5.118016103960565388, 11.49999999999999645 ) ) ;
#89480=CARTESIAN_POINT ( 'NONE',  ( -109.5228709571500616, -29.50250786944525672, 11.44777988621622988 ) ) ;
#89482=CARTESIAN_POINT ( 'NONE',  ( 5.627179592841175193, 21.36305014179116668, 11.49999999999998934 ) ) ;
#89483=CARTESIAN_POINT ( 'NONE',  ( -39.46140038746126777, -25.31589174274902376, 4.366343845060879580 ) ) ;
#89484=CARTESIAN_POINT ( 'NONE',  ( -47.62287095715004881, -23.47593901973091235, -1.443836447539009749 ) ) ;
#89485=DIRECTION ( 'NONE',  ( 0.000000000000000000, -2.173523156925979552E-06, 0.9999999999976378895 ) ) ;
#89487=CARTESIAN_POINT ( 'NONE',  ( -72.54967600462832422, -24.15543982623907127, -0.2315651400026662310 ) ) ;
#89488=CARTESIAN_POINT ( 'NONE',  ( -31.55269859854478653, -23.96119346886880663, -0.6495511937832003646 ) ) ;
#89489=ORIENTED_EDGE ( 'NONE', *, *, #12893, .F. ) ;
#89490=EDGE_LOOP ( 'NONE', ( #83727, #24347, #90510, #30783 ) ) ;
#89491=CARTESIAN_POINT ( 'NONE',  ( -41.58953762381673158, -23.48786465467240703, 11.44779295918255180 ) ) ;
#89492=CARTESIAN_POINT ( 'NONE',  ( -89.52287095715006160, -23.48786465467241769, 11.44779295918254292 ) ) ;
#89494=CARTESIAN_POINT ( 'NONE',  ( -17.31529204923715071, 11.11782870402162260, -1.500000000000002220 ) ) ;
#89495=CARTESIAN_POINT ( 'NONE',  ( -16.67190562677319932, -13.68652177170558204, 11.49999999999999645 ) ) ;
#89496=VERTEX_POINT ( 'NONE', #75782 ) ;
#89497=LINE ( 'NONE', #80390, #75292 ) ;
#89498=B_SPLINE_CURVE_WITH_KNOTS ( 'NONE', 3,
 ( #65044, #49808, #78707, #64044 ),
 .UNSPECIFIED., .F., .F.,
 ( 4, 4 ),
 ( 1.387778780781445521E-17, 0.0001000000000000028779 ),
 .UNSPECIFIED. ) ;
#89500=CARTESIAN_POINT ( 'NONE',  ( -35.62287095715004881, -23.48783264082477729, -1.443836473390072372 ) ) ;
#89501=CARTESIAN_POINT ( 'NONE',  ( 16.41691039316204481, 15.16158741987741365, 11.49999999999998934 ) ) ;
#89503=CARTESIAN_POINT ( 'NONE',  ( -32.68833172073793492, -25.12026506542017046, 2.831122744435439209 ) ) ;
#89504=VERTEX_POINT ( 'NONE', #67706 ) ;
#89507=CARTESIAN_POINT ( 'NONE',  ( 3.889286922045745776, 20.52237432693057073, -1.500000000000002220 ) ) ;
#89508=AXIS2_PLACEMENT_3D ( 'NONE', #6340, #59649, #37301 ) ;
#89509=VERTEX_POINT ( 'NONE', #12886 ) ;
#89510=FACE_OUTER_BOUND ( 'NONE', #66206, .T. ) ;
#89513=CARTESIAN_POINT ( 'NONE',  ( -51.25961469856053299, -25.27945219851612535, 4.204089154875919832 ) ) ;
#89514=CARTESIAN_POINT ( 'NONE',  ( 10.44912437418449969, 18.32051524777507723, -1.500000000000002220 ) ) ;
#89515=VERTEX_POINT ( 'NONE', #36738 ) ;
#89516=CARTESIAN_POINT ( 'NONE',  ( -28.52287095715006870, -24.17669640916165363, 0.1849426640301049252 ) ) ;
#89519=CARTESIAN_POINT ( 'NONE',  ( -120.5208167607407574, -23.85049219812686871, 10.88485053497526778 ) ) ;
#89520=ADVANCED_FACE ( 'NONE', ( #67207 ), #98623, .T. ) ;
#89522=CARTESIAN_POINT ( 'NONE',  ( -49.10800655684114702, -25.25745592776986825, 3.918720070390376176 ) ) ;
#89523=CARTESIAN_POINT ( 'NONE',  ( -19.66401359581072583, -9.230316601043258018, -1.500000000000002220 ) ) ;
#89525=CARTESIAN_POINT ( 'NONE',  ( -21.62769966018443313, 5.350386031573528989, 11.49999999999999645 ) ) ;
#89526=ORIENTED_EDGE ( 'NONE', *, *, #18721, .T. ) ;
#89527=CARTESIAN_POINT ( 'NONE',  ( -50.37830952628071657, -25.31441722265898875, 5.197788989113472979 ) ) ;
#89529=LINE ( 'NONE', #59094, #31025 ) ;
#89531=EDGE_CURVE ( 'NONE', #2820, #78888, #74787, .T. ) ;
#89533=CARTESIAN_POINT ( 'NONE',  ( -36.22287095715006444, -23.47596703998600276, 11.44779298504227683 ) ) ;
#89538=CARTESIAN_POINT ( 'NONE',  ( -75.52287095715007581, -24.52232992886362695, 0.6492154411906060352 ) ) ;
#89540=CARTESIAN_POINT ( 'NONE',  ( -103.5228709571500758, -24.65952944569304606, 1.056160979905702346 ) ) ;
#89541=FACE_OUTER_BOUND ( 'NONE', #43324, .T. ) ;
#89542=EDGE_CURVE ( 'NONE', #477, #2525, #21490, .T. ) ;
#89543=CARTESIAN_POINT ( 'NONE',  ( -66.52287095715004739, -23.95044443724993144, 10.65354141964649237 ) ) ;
#89545=CARTESIAN_POINT ( 'NONE',  ( 12.26431755764203047, -15.03328313062362298, 11.49999999999999645 ) ) ;
#89546=DIRECTION ( 'NONE',  ( -0.000000000000000000, 2.173523156925979552E-06, -0.9999999999976378895 ) ) ;
#89547=CARTESIAN_POINT ( 'NONE',  ( -1.649324495273077451, -22.40575143947253167, -1.500000000000002220 ) ) ;
#89550=FACE_OUTER_BOUND ( 'NONE', #63726, .T. ) ;
#89553=CARTESIAN_POINT ( 'NONE',  ( -63.92535995814584027, -24.57215472537218304, 9.174899246800711339 ) ) ;
#89554=CARTESIAN_POINT ( 'NONE',  ( 0.9049686737998731134, -19.58615294826029540, -1.500000000000002220 ) ) ;
#89555=B_SPLINE_SURFACE_WITH_KNOTS ( 'NONE', 3, 3, ( 
 ( #98078, #28094, #28584, #4261 ),
 ( #20461, #35210, #51433, #82369 ),
 ( #73274, #66683, #89488, #42340 ),
 ( #12353, #74263, #20961, #57560 ),
 ( #51932, #5247, #43326, #97594 ),
 ( #43816, #74751, #36205, #13347 ),
 ( #72779, #88496, #80881, #3768 ) ),
 .UNSPECIFIED., .F., .F., .F.,
 ( 4, 3, 4 ),
 ( 4, 4 ),
 ( 0.0004766839783831800718, 0.1029713700210899974, 0.2054660560637968092 ),
 ( 0.9897457716632639402, 0.9912151630997512175 ),
 .UNSPECIFIED. ) ;
#89556=CARTESIAN_POINT ( 'NONE',  ( -120.5228709571500616, -23.47596703998600631, 11.44779298504227860 ) ) ;
#89558=CARTESIAN_POINT ( 'NONE',  ( -11.74548148041400708, 18.04809798412036059, 11.49999999999998934 ) ) ;
#89560=CARTESIAN_POINT ( 'NONE',  ( -71.30376622360817862, -25.12218957384495965, 6.239614793150383143 ) ) ;
#89561=CARTESIAN_POINT ( 'NONE',  ( -75.52287095715007581, -23.48786465467241769, 11.44779295918254469 ) ) ;
#89562=B_SPLINE_CURVE_WITH_KNOTS ( 'NONE', 3,
 ( #99661, #21548, #75840, #30167 ),
 .UNSPECIFIED., .F., .F.,
 ( 4, 4 ),
 ( 0.000000000000000000, 9.999999999998898659E-05 ),
 .UNSPECIFIED. ) ;
#89563=LINE ( 'NONE', #2338, #79603 ) ;
#89564=CARTESIAN_POINT ( 'NONE',  ( 16.23347398924790497, -16.23827457187686463, -1.500000000000002220 ) ) ;
#89568=CARTESIAN_POINT ( 'NONE',  ( -49.58209155508411925, -24.51314013834316086, 0.6176544820404115121 ) ) ;
#89569=CARTESIAN_POINT ( 'NONE',  ( -1.972954090310384379, -20.06304030521763337, 11.49999999999999645 ) ) ;
#89570=CARTESIAN_POINT ( 'NONE',  ( -109.4252266130965552, -25.10927462135256150, 3.135431895769846822 ) ) ;
#89575=CARTESIAN_POINT ( 'NONE',  ( -46.62287095715004881, -29.50247984919015209, -1.443849546365058689 ) ) ;
#89576=CARTESIAN_POINT ( 'NONE',  ( -19.70454523906213495, -2.556213046838741842, 11.49999999999998934 ) ) ;
#89577=AXIS2_PLACEMENT_3D ( 'NONE', #96475, #3642, #26477 ) ;
#89578=CARTESIAN_POINT ( 'NONE',  ( -109.6228709571500559, -24.64898659630368627, 1.056161002820831474 ) ) ;
#89579=CARTESIAN_POINT ( 'NONE',  ( 2.169241753049089727, -19.58708112974024829, -1.500000000000002220 ) ) ;
#89580=EDGE_CURVE ( 'NONE', #46174, #81901, #47055, .T. ) ;
#89581=CARTESIAN_POINT ( 'NONE',  ( -126.5899057953276667, -24.15620529776629510, 10.23563542870658871 ) ) ;
#89582=AXIS2_PLACEMENT_3D ( 'NONE', #86442, #38759, #48388 ) ;
#89583=CARTESIAN_POINT ( 'NONE',  ( -110.5228709571500190, -24.14406661686757971, 10.28769366194080526 ) ) ;
#89584=CARTESIAN_POINT ( 'NONE',  ( -79.52287095715006160, -24.50321055353805377, 9.387540953477524042 ) ) ;
#89585=CARTESIAN_POINT ( 'NONE',  ( 20.28538307770854487, 3.844468116359331944, 11.49999999999999645 ) ) ;
#89588=CARTESIAN_POINT ( 'NONE',  ( -22.35490716430079061, -3.811827842488555440, 11.49999999999999645 ) ) ;
#89589=ORIENTED_EDGE ( 'NONE', *, *, #23311, .F. ) ;
#89592=CARTESIAN_POINT ( 'NONE',  ( -63.59273280689718888, -24.15543982623906771, -0.2315651400026651485 ) ) ;
#89593=PLANE ( 'NONE',  #22040 ) ;
#89594=ORIENTED_EDGE ( 'NONE', *, *, #6477, .T. ) ;
#89595=B_SPLINE_CURVE_WITH_KNOTS ( 'NONE', 3,
 ( #51500, #14412, #74330, #76304 ),
 .UNSPECIFIED., .F., .F.,
 ( 4, 4 ),
 ( 0.000000000000000000, 9.999999999998897304E-05 ),
 .UNSPECIFIED. ) ;
#89598=CARTESIAN_POINT ( 'NONE',  ( -30.51968327036646400, -23.47799326397811726, -1.443836481326576271 ) ) ;
#89599=CARTESIAN_POINT ( 'NONE',  ( 18.61037501828884189, -13.27421459584354579, -1.500000000000002220 ) ) ;
#89600=CARTESIAN_POINT ( 'NONE',  ( -130.5728709571500588, -23.56000036390796737, 11.50200000000000244 ) ) ;
#89601=CARTESIAN_POINT ( 'NONE',  ( 17.58597629297885589, -12.55149374826878272, -1.500000000000002220 ) ) ;
#89602=CARTESIAN_POINT ( 'NONE',  ( -113.5949056871682359, -23.48786465467241413, 11.44779295918254292 ) ) ;
#89603=LINE ( 'NONE', #82972, #77625 ) ;
#89605=CARTESIAN_POINT ( 'NONE',  ( -15.68175098440391402, -16.16561365185589594, 11.49999999999999645 ) ) ;
#89606=ORIENTED_EDGE ( 'NONE', *, *, #46743, .T. ) ;
#89607=CARTESIAN_POINT ( 'NONE',  ( -43.52287095715006160, -24.65952944569304606, 1.056160979905691910 ) ) ;
#89608=CARTESIAN_POINT ( 'NONE',  ( 21.96865551644221881, -1.217672407684077918, -1.500000000000002220 ) ) ;
#89610=CARTESIAN_POINT ( 'NONE',  ( -29.23483314410334444, -25.21724520516633561, 5.425066621826060143 ) ) ;
#89612=ORIENTED_EDGE ( 'NONE', *, *, #81422, .F. ) ;
#89613=FACE_OUTER_BOUND ( 'NONE', #56896, .T. ) ;
#89614=CARTESIAN_POINT ( 'NONE',  ( -47.62287095715006302, -23.47596703998600276, 11.44779298504227505 ) ) ;
#89617=VERTEX_POINT ( 'NONE', #20500 ) ;
#89618=ORIENTED_EDGE ( 'NONE', *, *, #65848, .F. ) ;
#89621=DIRECTION ( 'NONE',  ( -3.773278334453079618E-23, 0.9999999999976377785, 2.173523156925979975E-06 ) ) ;
#89622=LINE ( 'NONE', #52558, #71344 ) ;
#89623=CARTESIAN_POINT ( 'NONE',  ( -50.52287095715006160, -24.99132157543166599, 2.256160258750667502 ) ) ;
#89624=CARTESIAN_POINT ( 'NONE',  ( -4.163110563111144913, -19.98234244090558320, -1.500000000000002220 ) ) ;
#89625=ORIENTED_EDGE ( 'NONE', *, *, #47826, .T. ) ;
#89627=LINE ( 'NONE', #50566, #69262 ) ;
#89628=EDGE_CURVE ( 'NONE', #30676, #78152, #79742, .T. ) ;
#89629=CARTESIAN_POINT ( 'NONE',  ( -97.52287095715006160, -23.94994826722564341, -0.6494450866342716955 ) ) ;
#89630=CARTESIAN_POINT ( 'NONE',  ( -56.62287095715005592, -29.50250243563736774, 8.947779886222145151 ) ) ;
#89632=CARTESIAN_POINT ( 'NONE',  ( -83.62287095715007013, -23.47596703998600631, 11.44779298504227860 ) ) ;
#89633=FACE_OUTER_BOUND ( 'NONE', #48761, .T. ) ;
#89634=ORIENTED_EDGE ( 'NONE', *, *, #49906, .F. ) ;
#89635=CARTESIAN_POINT ( 'NONE',  ( -19.11632921840048738, -8.121837694355717119, -1.500000000000002220 ) ) ;
#89637=CARTESIAN_POINT ( 'NONE',  ( -53.52287095715006870, -29.50250243563736774, 8.947779886222146928 ) ) ;
#89638=ORIENTED_EDGE ( 'NONE', *, *, #78741, .T. ) ;
#89640=CARTESIAN_POINT ( 'NONE',  ( -44.55620429048338593, -23.47596703998600276, 11.44779298504227505 ) ) ;
#89641=CARTESIAN_POINT ( 'NONE',  ( -67.62287095715005592, -29.50248528299804818, 1.056150453629036701 ) ) ;
#89644=CARTESIAN_POINT ( 'NONE',  ( -79.62287095715004170, -24.65952944569304606, 1.056160979905697461 ) ) ;
#89645=EDGE_CURVE ( 'NONE', #38032, #37450, #65236, .T. ) ;
#89646=CARTESIAN_POINT ( 'NONE',  ( -123.5895376238167245, -24.64965694238408034, 8.947790433994649462 ) ) ;
#89647=CARTESIAN_POINT ( 'NONE',  ( -55.55620429048340014, -23.48783264082478439, -1.443836473390068820 ) ) ;
#89648=CARTESIAN_POINT ( 'NONE',  ( -71.30164606794451743, -25.24515217160483971, 6.118441223290502329 ) ) ;
#89649=CARTESIAN_POINT ( 'NONE',  ( 7.254013858510784729, 20.86747967231135803, 11.49999999999999645 ) ) ;
#89650=ORIENTED_EDGE ( 'NONE', *, *, #80746, .F. ) ;
#89654=CARTESIAN_POINT ( 'NONE',  ( 12.73759380600583846, -18.68238426224762350, 11.49999999999998934 ) ) ;
#89656=DIRECTION ( 'NONE',  ( 0.000000000000000000, -2.173523156925979552E-06, 0.9999999999976378895 ) ) ;
#89657=ORIENTED_EDGE ( 'NONE', *, *, #98921, .F. ) ;
#89658=AXIS2_PLACEMENT_3D ( 'NONE', #7828, #56025, #63137 ) ;
#89659=EDGE_CURVE ( 'NONE', #71190, #42155, #43859, .T. ) ;
#89661=EDGE_CURVE ( 'NONE', #43450, #33967, #83335, .T. ) ;
#89662=CARTESIAN_POINT ( 'NONE',  ( -80.43221577628075636, -25.31553502933635968, 4.967019755914117596 ) ) ;
#89664=ORIENTED_EDGE ( 'NONE', *, *, #20223, .F. ) ;
#89665=CARTESIAN_POINT ( 'NONE',  ( -17.67215177357914513, -11.65580189297658897, 11.49999999999998934 ) ) ;
#89668=CARTESIAN_POINT ( 'NONE',  ( 11.81759748825469281, -18.92407201980706333, -1.500000000000002220 ) ) ;
#89670=ADVANCED_FACE ( 'NONE', ( #51971 ), #76280, .F. ) ;
#89671=VERTEX_POINT ( 'NONE', #15379 ) ;
#89673=CARTESIAN_POINT ( 'NONE',  ( -50.62287095715005592, -23.47596703998600631, 11.44779298504227505 ) ) ;
#89676=AXIS2_PLACEMENT_3D ( 'NONE', #92315, #60398, #45654 ) ;
#89677=CARTESIAN_POINT ( 'NONE',  ( -13.79594968651775666, -13.80015156857029268, 11.49999999999998934 ) ) ;
#89678=CARTESIAN_POINT ( 'NONE',  ( -18.57871158907727249, 10.67946855401146777, -1.500000000000002220 ) ) ;
#89679=CARTESIAN_POINT ( 'NONE',  ( -27.65533724976895869, -24.92774666542950257, 1.629627248584496257 ) ) ;
#89682=CARTESIAN_POINT ( 'NONE',  ( -21.74551633039419585, 6.958787177381512201, -1.500000000000002220 ) ) ;
#89683=AXIS2_PLACEMENT_3D ( 'NONE', #45503, #14023, #60234 ) ;
#89685=DIRECTION ( 'NONE',  ( 0.000000000000000000, -0.9999999999976377785, -2.173523156925979975E-06 ) ) ;
#89686=DIRECTION ( 'NONE',  ( -3.773278334453079618E-23, 0.9999999999976377785, 2.173523156925979975E-06 ) ) ;
#89687=CARTESIAN_POINT ( 'NONE',  ( 19.23997954701083657, -5.074110557352235595, 11.49999999999999645 ) ) ;
#89688=CARTESIAN_POINT ( 'NONE',  ( -104.5928578189489855, -23.96119346886880663, -0.6495511937832033622 ) ) ;
#89690=CARTESIAN_POINT ( 'NONE',  ( -123.6228709571500559, -24.50216790748099527, 0.6166512839513689226 ) ) ;
#89691=CARTESIAN_POINT ( 'NONE',  ( -56.62287095715008434, -23.47596703998600276, 11.44779298504227683 ) ) ;
#89692=B_SPLINE_CURVE_WITH_KNOTS ( 'NONE', 3,
 ( #21143, #7797, #83038, #90172 ),
 .UNSPECIFIED., .F., .F.,
 ( 4, 4 ),
 ( 1.387778780781445521E-17, 9.999999999996123101E-05 ),
 .UNSPECIFIED. ) ;
#89696=CARTESIAN_POINT ( 'NONE',  ( -62.62287095715004881, -24.64965695001468404, 8.947790433994185832 ) ) ;
#89697=CARTESIAN_POINT ( 'NONE',  ( 13.45394552336293614, 17.01807010946250287, 11.49999999999998934 ) ) ;
#89699=B_SPLINE_CURVE_WITH_KNOTS ( 'NONE', 3,
 ( #47411, #78338, #84959, #77337, #38786, #228 ),
 .UNSPECIFIED., .F., .F.,
 ( 4, 2, 4 ),
 ( 0.000000000000000000, 0.001380764517854767134, 0.002761529035709534268 ),
 .UNSPECIFIED. ) ;
#89700=CARTESIAN_POINT ( 'NONE',  ( -12.82114019720147802, -14.77593736753402709, -1.500000000000002220 ) ) ;
#89701=B_SPLINE_CURVE_WITH_KNOTS ( 'NONE', 3,
 ( #94117, #63704, #64203, #86010, #79892, #70794 ),
 .UNSPECIFIED., .F., .F.,
 ( 4, 2, 4 ),
 ( 6.384118695823475424E-06, 0.001386860460836977695, 0.002767336802978131918 ),
 .UNSPECIFIED. ) ;
#89702=PLANE ( 'NONE',  #11810 ) ;
#89704=ORIENTED_EDGE ( 'NONE', *, *, #43077, .T. ) ;
#89706=B_SPLINE_CURVE_WITH_KNOTS ( 'NONE', 3,
 ( #98914, #77069, #7575, #76076, #99898, #61876, #60387, #38523 ),
 .UNSPECIFIED., .F., .F.,
 ( 4, 2, 2, 4 ),
 ( 6.391158118966157767E-06, 0.002007136338672926151, 0.003007508928949903862, 0.004007881519226882440 ),
 .UNSPECIFIED. ) ;
#89707=PLANE ( 'NONE',  #77496 ) ;
#89708=CARTESIAN_POINT ( 'NONE',  ( -18.53176153473302179, -8.692061069824589481, 11.49999999999999645 ) ) ;
#89709=CARTESIAN_POINT ( 'NONE',  ( -49.27764846858840997, -25.25176233969420636, 6.145204990682164414 ) ) ;
#89710=DIRECTION ( 'NONE',  ( -0.9970298735180330718, -0.07701578612606008178, -9.020562075079398124E-17 ) ) ;
#89711=VERTEX_POINT ( 'NONE', #8280 ) ;
#89712=EDGE_CURVE ( 'NONE', #37238, #18378, #55497, .T. ) ;
#89720=PLANE ( 'NONE',  #73932 ) ;
#89721=CARTESIAN_POINT ( 'NONE',  ( -20.90396053131702914, -9.656267258341529214, 11.49999999999999645 ) ) ;
#89722=CARTESIAN_POINT ( 'NONE',  ( 4.306090731860143350, 22.38281141545218844, 11.49999999999998934 ) ) ;
#89723=CARTESIAN_POINT ( 'NONE',  ( -70.66110687620329145, -25.30458803562652292, 4.882286574251741840 ) ) ;
#89725=CARTESIAN_POINT ( 'NONE',  ( -40.52287095715010423, -24.14321612903120950, -0.2833117244520996780 ) ) ;
#89726=CARTESIAN_POINT ( 'NONE',  ( -49.50841769935765768, -25.27292115247390569, 3.984447733149576898 ) ) ;
#89728=CARTESIAN_POINT ( 'NONE',  ( -69.47459837275444272, -25.20046511427854341, 6.675966739650351478 ) ) ;
#89729=CARTESIAN_POINT ( 'NONE',  ( 18.42579859434530931, 11.83097890990371148, -1.500000000000002220 ) ) ;
#89731=CARTESIAN_POINT ( 'NONE',  ( -82.62287095715005592, -29.50250243563736774, 8.947779886222141599 ) ) ;
#89732=PLANE ( 'NONE',  #47648 ) ;
#89733=CARTESIAN_POINT ( 'NONE',  ( -120.6228709571500133, -24.14321612903117753, -0.2833117244520986233 ) ) ;
#89734=LINE ( 'NONE', #13088, #76054 ) ;
#89735=ORIENTED_EDGE ( 'NONE', *, *, #83269, .F. ) ;
#89736=B_SPLINE_CURVE_WITH_KNOTS ( 'NONE', 3,
 ( #17947, #42592, #24458, #43579, #89752, #34468, #74518, #63044 ),
 .UNSPECIFIED., .F., .F.,
 ( 4, 2, 2, 4 ),
 ( -0.001240666984355843008, -0.0002401179793395007492, 0.0007604310256768415099, 0.002761529035709526028 ),
 .UNSPECIFIED. ) ;
#89737=CARTESIAN_POINT ( 'NONE',  ( 3.609400094169940676, -20.08663944828865766, 11.49999999999998934 ) ) ;
#89741=ORIENTED_EDGE ( 'NONE', *, *, #59997, .T. ) ;
#89742=CARTESIAN_POINT ( 'NONE',  ( -21.75560140871883164, 7.562747417745157463, -1.500000000000002220 ) ) ;
#89743=CARTESIAN_POINT ( 'NONE',  ( -34.62287095715005592, -29.50250786944525672, 11.44777988621624409 ) ) ;
#89744=CARTESIAN_POINT ( 'NONE',  ( 20.17645099164838030, 1.678240329834772115, -1.500000000000002220 ) ) ;
#89745=ORIENTED_EDGE ( 'NONE', *, *, #56660, .F. ) ;
#89747=CARTESIAN_POINT ( 'NONE',  ( -78.22287095715006444, -23.47596703998600631, 11.44779298504227860 ) ) ;
#89748=CARTESIAN_POINT ( 'NONE',  ( -51.62287095715005592, -23.47596703998600631, 11.44779298504227505 ) ) ;
#89750=CARTESIAN_POINT ( 'NONE',  ( -7.638042729800005759, 19.97414216180626667, 11.49999999999999645 ) ) ;
#89752=CARTESIAN_POINT ( 'NONE',  ( -55.52287095715007581, -24.51163499207173402, 0.6490370598554341397 ) ) ;
#89754=CARTESIAN_POINT ( 'NONE',  ( 14.93699691249320693, 16.48547057857716425, 11.49999999999998934 ) ) ;
#89755=CARTESIAN_POINT ( 'NONE',  ( -6.067718162532647064, 19.77315050736717694, 11.49999999999998934 ) ) ;
#89760=CARTESIAN_POINT ( 'NONE',  ( -56.52287095715004739, -23.94994826722565406, -0.6494450866342736939 ) ) ;
#89762=VECTOR ( 'NONE', #950, 1000.000000000000114 ) ;
#89763=CARTESIAN_POINT ( 'NONE',  ( -13.90609606471210391, -15.62508359690603221, -1.500000000000002220 ) ) ;
#89765=CARTESIAN_POINT ( 'NONE',  ( 19.94191871449930531, -9.063712221575384476, 11.49999999999999645 ) ) ;
#89766=CARTESIAN_POINT ( 'NONE',  ( -37.59388924453935488, -24.15620529776627379, 10.23563542870660825 ) ) ;
#89767=CARTESIAN_POINT ( 'NONE',  ( -18.84819291449097278, 12.34854029719970825, -1.500000000000002220 ) ) ;
#89768=CARTESIAN_POINT ( 'NONE',  ( 5.581485548573628996, 20.18083795961418403, 11.49999999999998934 ) ) ;
#89769=DIRECTION ( 'NONE',  ( -1.000000000000000000, -3.773278334444167608E-23, -8.201307833595939069E-29 ) ) ;
#89771=CARTESIAN_POINT ( 'NONE',  ( -119.5532575478694071, -24.51419770103158768, 9.386484678747164523 ) ) ;
#89773=VERTEX_POINT ( 'NONE', #100098 ) ;
#89776=B_SPLINE_CURVE_WITH_KNOTS ( 'NONE', 3,
 ( #23338, #8141, #85248, #94866 ),
 .UNSPECIFIED., .F., .F.,
 ( 4, 4 ),
 ( 0.000000000000000000, 9.999999999998897304E-05 ),
 .UNSPECIFIED. ) ;
#89777=ORIENTED_EDGE ( 'NONE', *, *, #51482, .F. ) ;
#89778=EDGE_CURVE ( 'NONE', #81148, #11463, #29956, .T. ) ;
#89780=CARTESIAN_POINT ( 'NONE',  ( -12.84383942963603964, -17.20202612561282862, -1.500000000000002220 ) ) ;
#89782=EDGE_LOOP ( 'NONE', ( #76373, #49115, #26928, #41474, #80548, #51434 ) ) ;
#89783=CARTESIAN_POINT ( 'NONE',  ( 19.39439428382967634, -8.317090367284466268, -1.500000000000002220 ) ) ;
#89784=CARTESIAN_POINT ( 'NONE',  ( -99.91756162674147390, -25.21046098787585521, 3.405294827540925606 ) ) ;
#89785=CARTESIAN_POINT ( 'NONE',  ( -37.62287095715005592, -23.48783264082477373, -1.443836473390072372 ) ) ;
#89786=CARTESIAN_POINT ( 'NONE',  ( -109.6228709571500559, -24.64898659630368627, 1.056161002820831474 ) ) ;
#89787=DIRECTION ( 'NONE',  ( 3.773278334444167608E-23, -1.000000000000000000, 0.000000000000000000 ) ) ;
#89789=CARTESIAN_POINT ( 'NONE',  ( 18.88560736741940005, 11.47387103136259690, -1.500000000000002220 ) ) ;
#89790=CARTESIAN_POINT ( 'NONE',  ( -101.6228709571500559, -29.50250786944525672, 11.44777988621623166 ) ) ;
#89791=ADVANCED_FACE ( 'NONE', ( #86403 ), #14882, .F. ) ;
#89794=CARTESIAN_POINT ( 'NONE',  ( -78.62287095715004170, -23.48786465467241413, 11.44779295918254469 ) ) ;
#89796=AXIS2_PLACEMENT_3D ( 'NONE', #21446, #30068, #99564 ) ;
#89797=CARTESIAN_POINT ( 'NONE',  ( 20.65877813657638740, 5.380652674160894655, 11.49999999999998934 ) ) ;
#89799=CARTESIAN_POINT ( 'NONE',  ( -48.86012939852317771, -25.11539320716599377, 2.804431449967496714 ) ) ;
#89800=CARTESIAN_POINT ( 'NONE',  ( -84.62287095715005592, -24.66019654487199730, 8.947790411086128159 ) ) ;
#89802=CARTESIAN_POINT ( 'NONE',  ( -22.13905560727926414, 4.690293145198261904, -1.500000000000002220 ) ) ;
#89803=ORIENTED_EDGE ( 'NONE', *, *, #34229, .F. ) ;
#89805=CARTESIAN_POINT ( 'NONE',  ( -79.55873559869328915, -23.73766607897669800, -1.055555164236459564 ) ) ;
#89806=CARTESIAN_POINT ( 'NONE',  ( -19.30086548479123465, -4.275078920326023990, 11.49999999999999645 ) ) ;
#89807=DIRECTION ( 'NONE',  ( -3.773278334453079030E-23, 0.9999999999976377785, 2.173523156925979128E-06 ) ) ;
#89808=CARTESIAN_POINT ( 'NONE',  ( -67.51047822507001683, -23.96119346886879953, -0.6495511937832114668 ) ) ;
#89809=VERTEX_POINT ( 'NONE', #71188 ) ;
#89810=DIRECTION ( 'NONE',  ( 3.773278334444167608E-23, -1.000000000000000000, 0.000000000000000000 ) ) ;
#89811=CARTESIAN_POINT ( 'NONE',  ( -29.47844009783932862, -25.26026551470690507, 2.848994710608491854 ) ) ;
#89813=CARTESIAN_POINT ( 'NONE',  ( 10.18377579766961283, -19.05927572544859672, -1.500000000000002220 ) ) ;
#89814=CARTESIAN_POINT ( 'NONE',  ( -49.36186039879741116, -25.10935227259399127, 3.293515131321622658 ) ) ;
#89815=CARTESIAN_POINT ( 'NONE',  ( -5.843762028675351772, -18.45606589188993141, -1.500000000000002220 ) ) ;
#89818=CARTESIAN_POINT ( 'NONE',  ( -17.81549539028256746, -8.563599010019245839, 11.49999999999998934 ) ) ;
#89821=CARTESIAN_POINT ( 'NONE',  ( -16.53579703214142427, -11.71821515807347680, 11.49999999999999645 ) ) ;
#89822=PLANE ( 'NONE',  #91043 ) ;
#89826=EDGE_LOOP ( 'NONE', ( #87526, #17231, #27338, #2392 ) ) ;
#89827=B_SPLINE_SURFACE_WITH_KNOTS ( 'NONE', 3, 3, ( 
 ( #67781, #98699, #35814, #67275 ),
 ( #82969, #12470, #74369, #52536 ),
 ( #97706, #28200, #59663, #90101 ),
 ( #90593, #20575, #28703, #82478 ),
 ( #12958, #74857, #21564, #21072 ),
 ( #52040, #75357, #5857, #83472 ),
 ( #29195, #13959, #46415, #1252 ) ),
 .UNSPECIFIED., .F., .F., .F.,
 ( 4, 3, 4 ),
 ( 4, 4 ),
 ( 0.0004767105685617169480, 0.1029713956399723879, 0.2054660807113830590 ),
 ( 0.03212754048487516390, 0.03698070728729284384 ),
 .UNSPECIFIED. ) ;
#89828=CARTESIAN_POINT ( 'NONE',  ( -110.5562042904833930, -24.99132157543166954, 2.256160258750667946 ) ) ;
#89830=CARTESIAN_POINT ( 'NONE',  ( -71.52287095715009002, -24.51387760970726148, 9.387446482453414731 ) ) ;
#89832=B_SPLINE_CURVE_WITH_KNOTS ( 'NONE', 3,
 ( #40675, #11219, #87846, #17324, #25439, #10219 ),
 .UNSPECIFIED., .F., .F.,
 ( 4, 2, 4 ),
 ( 1.570755371634033063E-05, 0.001396183895866089921, 0.002776660238015839482 ),
 .UNSPECIFIED. ) ;
#89833=CARTESIAN_POINT ( 'NONE',  ( -53.52287095715006870, -29.50247984919015209, -1.443849546365058689 ) ) ;
#89834=CARTESIAN_POINT ( 'NONE',  ( 19.70663390988245922, 3.666079223618853966, 11.49999999999998934 ) ) ;
#89836=EDGE_LOOP ( 'NONE', ( #34965, #52456, #82483, #43435 ) ) ;
#89837=CARTESIAN_POINT ( 'NONE',  ( -103.5228709571500758, -23.48786465467241769, 11.44779295918254114 ) ) ;
#89838=LINE ( 'NONE', #29427, #10532 ) ;
#89839=CARTESIAN_POINT ( 'NONE',  ( -89.81226385320384509, -25.06732983082694943, 7.447789526168956620 ) ) ;
#89840=DIRECTION ( 'NONE',  ( -0.000000000000000000, 2.173523156925979552E-06, -0.9999999999976378895 ) ) ;
#89843=EDGE_CURVE ( 'NONE', #16634, #53307, #75959, .T. ) ;
#89845=CARTESIAN_POINT ( 'NONE',  ( -50.02146468009372171, -25.30419751004783535, 5.186272124421678953 ) ) ;
#89846=ORIENTED_EDGE ( 'NONE', *, *, #6637, .F. ) ;
#89847=CARTESIAN_POINT ( 'NONE',  ( -9.641467040090685003, 17.89903724589931855, 11.49999999999998934 ) ) ;
#89848=VERTEX_POINT ( 'NONE', #55973 ) ;
#89849=CARTESIAN_POINT ( 'NONE',  ( 22.95104020007722667, -0.4190376320207603866, 11.49999999999998934 ) ) ;
#89850=CARTESIAN_POINT ( 'NONE',  ( -32.62373917829282988, -24.65952944569304606, 1.056160979905696351 ) ) ;
#89852=ADVANCED_FACE ( 'NONE', ( #95015 ), #49868, .T. ) ;
#89853=ORIENTED_EDGE ( 'NONE', *, *, #86992, .T. ) ;
#89854=CARTESIAN_POINT ( 'NONE',  ( -108.5228709571501042, -24.66019654487200441, 8.947790411086113949 ) ) ;
#89855=EDGE_CURVE ( 'NONE', #76180, #72299, #91778, .T. ) ;
#89856=CARTESIAN_POINT ( 'NONE',  ( -49.27993637813898431, -25.26263991058249658, 6.239168797676713396 ) ) ;
#89858=CARTESIAN_POINT ( 'NONE',  ( 3.302162439418223627, -20.95225242093645690, 11.49999999999999645 ) ) ;
#89859=VERTEX_POINT ( 'NONE', #26004 ) ;
#89861=CARTESIAN_POINT ( 'NONE',  ( -14.73459587841175633, -16.56598928932902837, 11.49999999999998934 ) ) ;
#89862=CARTESIAN_POINT ( 'NONE',  ( 17.30552477474510908, -11.17933342135444086, 11.49999999999998934 ) ) ;
#89868=ORIENTED_EDGE ( 'NONE', *, *, #86852, .T. ) ;
#89869=ORIENTED_EDGE ( 'NONE', *, *, #42780, .F. ) ;
#89870=CARTESIAN_POINT ( 'NONE',  ( -111.7766730966630604, -25.29170726702208682, 4.234259702825696969 ) ) ;
#89873=CARTESIAN_POINT ( 'NONE',  ( 20.56943099487245519, -2.726235779781958968, -1.500000000000002220 ) ) ;
#89875=CARTESIAN_POINT ( 'NONE',  ( -21.04499429308205549, 5.405531755741471045, 11.49999999999999645 ) ) ;
#89876=ORIENTED_EDGE ( 'NONE', *, *, #23466, .T. ) ;
#89877=PLANE ( 'NONE',  #39615 ) ;
#89878=CARTESIAN_POINT ( 'NONE',  ( -77.58953762381673869, -23.48786465467241413, 11.44779295918254469 ) ) ;
#89879=CARTESIAN_POINT ( 'NONE',  ( -115.5522256392173261, -24.63355581998386157, 0.9682620441943915468 ) ) ;
#89880=CARTESIAN_POINT ( 'NONE',  ( -5.254942042970298210, 21.81482460008805546, 11.49999999999998934 ) ) ;
#89881=B_SPLINE_CURVE_WITH_KNOTS ( 'NONE', 3,
 ( #20488, #59079, #68177, #89513, #89021, #97126, #19497, #67692, #98611, #11888, #50457, #29103, #58087, #59577 ),
 .UNSPECIFIED., .F., .F.,
 ( 4, 2, 2, 2, 2, 2, 4 ),
 ( 8.673617379884035472E-19, 0.0001608593726895868325, 0.0003217187453791727977, 0.0006434374907583468965, 0.0009651562361375208869, 0.001126015608827097636, 0.001286874981516674277 ),
 .UNSPECIFIED. ) ;
#89883=CARTESIAN_POINT ( 'NONE',  ( -65.58633529694422748, -24.63355581998386867, 0.9682620441943842193 ) ) ;
#89885=CARTESIAN_POINT ( 'NONE',  ( -70.62287095715007013, -23.47596703998600631, 11.44779298504227505 ) ) ;
#89886=CARTESIAN_POINT ( 'NONE',  ( -93.62287095715005592, -24.64898659630367916, 1.056161002820827921 ) ) ;
#89888=EDGE_LOOP ( 'NONE', ( #87603, #43694, #70391, #56935 ) ) ;
#89889=VERTEX_POINT ( 'NONE', #11777 ) ;
#89890=CARTESIAN_POINT ( 'NONE',  ( -69.62287095715005592, -23.48786465467241058, 11.44779295918254824 ) ) ;
#89891=EDGE_CURVE ( 'NONE', #2274, #76771, #42750, .T. ) ;
#89893=CARTESIAN_POINT ( 'NONE',  ( -20.14006130340733236, -7.001243683211865410, -1.500000000000002220 ) ) ;
#89895=ORIENTED_EDGE ( 'NONE', *, *, #74997, .T. ) ;
#89896=CARTESIAN_POINT ( 'NONE',  ( -80.55620429048337883, -25.00182538069145721, 7.747789668545097541 ) ) ;
#89897=CARTESIAN_POINT ( 'NONE',  ( 12.58402814888991372, -17.87355554032721372, -1.500000000000002220 ) ) ;
#89899=CARTESIAN_POINT ( 'NONE',  ( 22.70222466501550329, 0.2752559529566028229, 11.49999999999998934 ) ) ;
#89902=CARTESIAN_POINT ( 'NONE',  ( 21.77894307773758698, -2.757304969434911879, -1.500000000000002220 ) ) ;
#89904=ORIENTED_EDGE ( 'NONE', *, *, #31678, .T. ) ;
#89906=CARTESIAN_POINT ( 'NONE',  ( -49.13273521788515552, -25.12782683882157642, 6.968846603086977787 ) ) ;
#89909=ORIENTED_EDGE ( 'NONE', *, *, #45488, .T. ) ;
#89912=CARTESIAN_POINT ( 'NONE',  ( -0.008165992925886865830, -22.94428480439657037, 3.856996771330998719 ) ) ;
#89913=CARTESIAN_POINT ( 'NONE',  ( -20.48789480994130230, 5.740754632170482097, 11.49999999999998934 ) ) ;
#89914=CARTESIAN_POINT ( 'NONE',  ( -112.6270366129879790, -24.15543982623908192, -0.2315651400026420559 ) ) ;
#89915=CARTESIAN_POINT ( 'NONE',  ( -26.14706027629300422, -24.97064798144177900, 4.097424676804005017 ) ) ;
#89917=CARTESIAN_POINT ( 'NONE',  ( -85.54877897942525067, -24.40034930558991277, 0.3402023900116044608 ) ) ;
#89921=CARTESIAN_POINT ( 'NONE',  ( -2.459534284235005863, 19.42625828800391119, 11.49999999999999645 ) ) ;
#89922=CARTESIAN_POINT ( 'NONE',  ( -108.5228709571500616, -24.64965694238408034, 8.947790433994192938 ) ) ;
#89923=CARTESIAN_POINT ( 'NONE',  ( -68.55620429048339304, -24.64898659630528854, 1.056161002820824368 ) ) ;
#89924=VERTEX_POINT ( 'NONE', #60472 ) ;
#89925=B_SPLINE_CURVE_WITH_KNOTS ( 'NONE', 3,
 ( #83297, #38121, #99510, #8185, #92906, #16290, #6675, #31515 ),
 .UNSPECIFIED., .F., .F.,
 ( 4, 2, 2, 4 ),
 ( -0.001224873891641412851, -0.0002244903592271006894, 0.0007758931731872114722, 0.002776660238015839048 ),
 .UNSPECIFIED. ) ;
#89927=CARTESIAN_POINT ( 'NONE',  ( -117.5228709571500758, -24.64965694238408034, 8.947790433994191162 ) ) ;
#89928=CARTESIAN_POINT ( 'NONE',  ( -101.9127759831245612, -25.22330154418774129, 6.417289855096420581 ) ) ;
#89929=CARTESIAN_POINT ( 'NONE',  ( -42.62287095715004881, -23.48783264082477373, -1.443836473390072817 ) ) ;
#89930=CARTESIAN_POINT ( 'NONE',  ( -45.62287095715004170, -24.51163499207174468, 0.6490370598554238146 ) ) ;
#89931=ADVANCED_FACE ( 'NONE', ( #19879 ), #97101, .T. ) ;
#89932=CARTESIAN_POINT ( 'NONE',  ( -8.027368788987615744, 17.96763083595211441, -1.500000000000002220 ) ) ;
#89935=CARTESIAN_POINT ( 'NONE',  ( -58.87764846858842560, -25.13069340115296058, 2.947789388436138580 ) ) ;
#89939=CARTESIAN_POINT ( 'NONE',  ( -87.52287095715006160, -24.64965694238575011, 8.947790433994196491 ) ) ;
#89940=CARTESIAN_POINT ( 'NONE',  ( -47.56852929004255515, -23.48783264082478084, -1.443836473390071706 ) ) ;
#89941=CARTESIAN_POINT ( 'NONE',  ( -118.6258448024444334, -24.15543982623907837, -0.2315651400026558782 ) ) ;
#89943=CARTESIAN_POINT ( 'NONE',  ( -70.25652273905276957, -25.31201591132865403, 5.316156949182883729 ) ) ;
#89944=CARTESIAN_POINT ( 'NONE',  ( -107.5924963967767667, -23.96119346886881374, -0.6495511937831857097 ) ) ;
#89945=CARTESIAN_POINT ( 'NONE',  ( -14.87316555497233495, -13.31901947624662519, 11.49999999999998934 ) ) ;
#89947=CARTESIAN_POINT ( 'NONE',  ( -0.09833458469086159282, -21.77698152587677427, -0.5187616176870144535 ) ) ;
#89948=VERTEX_POINT ( 'NONE', #59459 ) ;
#89949=CARTESIAN_POINT ( 'NONE',  ( -116.5895376238167103, -23.47596703998600631, 11.44779298504227683 ) ) ;
#89955=CARTESIAN_POINT ( 'NONE',  ( -107.5562042904833788, -24.66019654487200441, 8.947790411086124607 ) ) ;
#89956=B_SPLINE_CURVE_WITH_KNOTS ( 'NONE', 3,
 ( #18857, #74638, #58440, #10755, #49835, #89374 ),
 .UNSPECIFIED., .F., .F.,
 ( 4, 2, 4 ),
 ( 1.570755371633679342E-05, 0.001396183895866085151, 0.002776660238015833410 ),
 .UNSPECIFIED. ) ;
#89958=CARTESIAN_POINT ( 'NONE',  ( -49.62287095715005592, -23.47593901973091235, -1.443836447539009749 ) ) ;
#89959=EDGE_LOOP ( 'NONE', ( #47784, #73870, #61314, #13795 ) ) ;
#89960=EDGE_CURVE ( 'NONE', #66785, #92874, #89275, .T. ) ;
#89961=PLANE ( 'NONE',  #93278 ) ;
#89962=CARTESIAN_POINT ( 'NONE',  ( -127.5900869156286745, -23.96119346886880663, -0.6495511937832001426 ) ) ;
#89965=CARTESIAN_POINT ( 'NONE',  ( 5.465678960246475704, -19.50585317057041124, -1.500000000000002220 ) ) ;
#89967=CARTESIAN_POINT ( 'NONE',  ( -129.6228709571500701, -23.72747288104470442, -1.053458166803223683 ) ) ;
#89968=EDGE_CURVE ( 'NONE', #62568, #88839, #15388, .T. ) ;
#89969=EDGE_CURVE ( 'NONE', #19969, #30940, #84277, .T. ) ;
#89970=CARTESIAN_POINT ( 'NONE',  ( -76.62287095715007013, -24.65952944569304606, 1.056160979905700126 ) ) ;
#89973=CARTESIAN_POINT ( 'NONE',  ( -77.52287095715006160, -24.50321055353804311, 9.387540953477509831 ) ) ;
#89975=CARTESIAN_POINT ( 'NONE',  ( -4.751880754313710042, -19.48972053015312866, -1.500000000000002220 ) ) ;
#89976=CARTESIAN_POINT ( 'NONE',  ( 18.71565868802652588, -9.641079743366450572, 11.49999999999999645 ) ) ;
#89977=ADVANCED_FACE ( 'NONE', ( #23365 ), #31999, .F. ) ;
#89979=DIRECTION ( 'NONE',  ( -3.773278334453079030E-23, 0.9999999999976377785, 2.173523156925979128E-06 ) ) ;
#89980=CARTESIAN_POINT ( 'NONE',  ( 20.41560922187292348, 8.460057656491983380, -1.500000000000002220 ) ) ;
#89983=CARTESIAN_POINT ( 'NONE',  ( -47.62287095715004170, -23.72747288104469732, -1.053458166803227236 ) ) ;
#89984=PLANE ( 'NONE',  #42799 ) ;
#89986=CARTESIAN_POINT ( 'NONE',  ( -69.62287095715005592, -23.47593901973091235, -1.443836447539006196 ) ) ;
#89989=VERTEX_POINT ( 'NONE', #78651 ) ;
#89990=CARTESIAN_POINT ( 'NONE',  ( -55.52287095715006160, -23.85196035786899671, -0.8779234886475230093 ) ) ;
#89992=CARTESIAN_POINT ( 'NONE',  ( -61.62287095715004881, -23.47593901973091235, -1.443836447539007972 ) ) ;
#89993=CARTESIAN_POINT ( 'NONE',  ( -9.157874670058189892, -18.46812626297970539, -1.500000000000002220 ) ) ;
#89996=CARTESIAN_POINT ( 'NONE',  ( 4.073501596442082651, -21.17334570714589859, 11.49999999999999645 ) ) ;
#89998=CARTESIAN_POINT ( 'NONE',  ( -83.62287095715009855, -24.33927499327854704, 9.819080762295815390 ) ) ;
#89999=DIRECTION ( 'NONE',  ( -3.773278334453079618E-23, 0.9999999999976377785, 2.173523156925979975E-06 ) ) ;
#90001=CARTESIAN_POINT ( 'NONE',  ( 17.53502452033532677, 13.85421504792973479, -1.500000000000002220 ) ) ;
#90003=CARTESIAN_POINT ( 'NONE',  ( -59.62287095715006302, -23.48786465467241058, 11.44779295918254824 ) ) ;
#90004=CARTESIAN_POINT ( 'NONE',  ( -50.40445135320378967, -25.13313949306887451, 7.101635536975466678 ) ) ;
#90005=EDGE_CURVE ( 'NONE', #88484, #50353, #36075, .T. ) ;
#90007=CARTESIAN_POINT ( 'NONE',  ( -124.5228709571500616, -29.50247984919015209, -1.443849546365046699 ) ) ;
#90010=CARTESIAN_POINT ( 'NONE',  ( -20.82246440549779720, 1.468558417816581807, 11.49999999999998934 ) ) ;
#90013=EDGE_CURVE ( 'NONE', #66931, #20120, #9479, .T. ) ;
#90015=ORIENTED_EDGE ( 'NONE', *, *, #37, .F. ) ;
#90016=CARTESIAN_POINT ( 'NONE',  ( -100.5881548977521618, -24.63419186844610920, 9.035850630976920428 ) ) ;
#90017=CARTESIAN_POINT ( 'NONE',  ( -9.620199658202244208, 18.81650055922726494, -1.500000000000002220 ) ) ;
#90019=CARTESIAN_POINT ( 'NONE',  ( -91.62287095715004170, -24.66019654487199730, 8.947790411086124607 ) ) ;
#90020=CARTESIAN_POINT ( 'NONE',  ( -49.46295085228823751, -25.30521617469763740, 5.104712615514442220 ) ) ;
#90021=CARTESIAN_POINT ( 'NONE',  ( -48.62287095715007723, -24.35013146730204170, 9.818937971375113705 ) ) ;
#90022=CARTESIAN_POINT ( 'NONE',  ( -67.62287095715005592, -23.47593901973091235, -1.443836447539006196 ) ) ;
#90023=CARTESIAN_POINT ( 'NONE',  ( -50.38191529551148307, -25.11033443737753146, 2.832404817301930056 ) ) ;
#90024=CARTESIAN_POINT ( 'NONE',  ( -19.23829340896090656, 10.21096329589227025, -1.500000000000002220 ) ) ;
#90025=CARTESIAN_POINT ( 'NONE',  ( -81.41053730768496166, -25.12224268930417992, 6.535219352663868442 ) ) ;
#90026=CARTESIAN_POINT ( 'NONE',  ( -10.99827004860668822, -19.42154297629913628, 11.49999999999999645 ) ) ;
#90027=VERTEX_POINT ( 'NONE', #93387 ) ;
#90028=CARTESIAN_POINT ( 'NONE',  ( -57.52287095715004739, -24.35013146730203104, 9.818937971375106599 ) ) ;
#90031=EDGE_CURVE ( 'NONE', #70518, #38515, #53847, .T. ) ;
#90035=ADVANCED_FACE ( 'NONE', ( #84778 ), #54349, .T. ) ;
#90038=CARTESIAN_POINT ( 'NONE',  ( -75.52287095715006160, -25.00158670708909625, 2.256160236439166411 ) ) ;
#90041=B_SPLINE_CURVE_WITH_KNOTS ( 'NONE', 3,
 ( #8536, #70437, #68932, #46102, #45603, #37982 ),
 .UNSPECIFIED., .F., .F.,
 ( 4, 2, 4 ),
 ( 0.000000000000000000, 0.001380901958385393966, 0.002761803916770787931 ),
 .UNSPECIFIED. ) ;
#90042=CARTESIAN_POINT ( 'NONE',  ( -50.40895856474225667, -25.04307398257883577, 7.563174194274489892 ) ) ;
#90046=CARTESIAN_POINT ( 'NONE',  ( 19.02374887324148389, -3.781047496429098764, 11.49999999999999645 ) ) ;
#90047=CARTESIAN_POINT ( 'NONE',  ( -81.55620429048340725, -23.47596703998600276, 11.44779298504227683 ) ) ;
#90053=CARTESIAN_POINT ( 'NONE',  ( 13.97609912898263573, 13.72534901313461653, 11.49999999999998934 ) ) ;
#90054=CARTESIAN_POINT ( 'NONE',  ( -50.37830952628070946, -25.30401792888237367, 5.197789011716579033 ) ) ;
#90055=EDGE_LOOP ( 'NONE', ( #13001, #63854, #24407, #55456 ) ) ;
#90056=CARTESIAN_POINT ( 'NONE',  ( 13.05104812959431548, -17.15854754814989391, -1.500000000000002220 ) ) ;
#90057=CARTESIAN_POINT ( 'NONE',  ( -56.58953762381673158, -24.64898659630528499, 1.056161002820821704 ) ) ;
#90058=CARTESIAN_POINT ( 'NONE',  ( -69.52287095715006160, -23.48786465467241058, 11.44779295918254647 ) ) ;
#90059=CARTESIAN_POINT ( 'NONE',  ( -40.56084634221592466, -23.85016227208580730, -0.8807180028928395243 ) ) ;
#90060=CARTESIAN_POINT ( 'NONE',  ( -104.5228709571500758, -29.50248528299804818, 1.056150453629042030 ) ) ;
#90061=CARTESIAN_POINT ( 'NONE',  ( 0.2859537766682072601, -23.01552763051285666, -1.500000000000002220 ) ) ;
#90066=CARTESIAN_POINT ( 'NONE',  ( 18.53703574427524359, 7.882278514257341051, 11.49999999999999645 ) ) ;
#90067=CARTESIAN_POINT ( 'NONE',  ( -66.62287095715005592, -23.47596703998600276, 11.44779298504227683 ) ) ;
#90068=CARTESIAN_POINT ( 'NONE',  ( -120.6228709571500559, -25.00182538069145721, 7.747789668545100206 ) ) ;
#90069=VECTOR ( 'NONE', #3187, 1000.000000000000114 ) ;
#90074=CARTESIAN_POINT ( 'NONE',  ( -10.37884456512175291, 16.95428827495986823, 11.49999999999998934 ) ) ;
#90077=CARTESIAN_POINT ( 'NONE',  ( 18.87426695099163254, 5.791883100666666451, -1.500000000000002220 ) ) ;
#90079=CARTESIAN_POINT ( 'NONE',  ( -126.5208993246462512, -24.35071581493544102, 9.817618358456011052 ) ) ;
#90083=CARTESIAN_POINT ( 'NONE',  ( 12.06641648444584369, 16.80774221200798735, 11.49999999999999645 ) ) ;
#90084=CARTESIAN_POINT ( 'NONE',  ( -53.55620429048340014, -24.66019654487199020, 8.947790411086135265 ) ) ;
#90085=LINE ( 'NONE', #74843, #69120 ) ;
#90086=CARTESIAN_POINT ( 'NONE',  ( -5.639450322166912777, -21.95568564230989850, 11.49999999999999645 ) ) ;
#90087=ORIENTED_EDGE ( 'NONE', *, *, #29261, .F. ) ;
#90088=LINE ( 'NONE', #87721, #77051 ) ;
#90089=CARTESIAN_POINT ( 'NONE',  ( -56.52287095715005449, -23.47593901973090169, -1.443836447538996870 ) ) ;
#90091=EDGE_CURVE ( 'NONE', #99101, #84227, #2124, .T. ) ;
#90092=FACE_OUTER_BOUND ( 'NONE', #92512, .T. ) ;
#90093=EDGE_CURVE ( 'NONE', #90831, #59375, #77157, .T. ) ;
#90096=ORIENTED_EDGE ( 'NONE', *, *, #20038, .T. ) ;
#90099=DIRECTION ( 'NONE',  ( -0.000000000000000000, 2.173523156925979552E-06, -0.9999999999976378895 ) ) ;
#90100=CARTESIAN_POINT ( 'NONE',  ( -22.64140897529919272, -3.284158816904186651, -1.500000000000002220 ) ) ;
#90101=CARTESIAN_POINT ( 'NONE',  ( -29.50322070279044340, -23.87424752075005330, -0.6495508823503305385 ) ) ;
#90102=CARTESIAN_POINT ( 'NONE',  ( -13.10987527212420645, -17.12674121770768920, -1.500000000000002220 ) ) ;
#90103=CARTESIAN_POINT ( 'NONE',  ( -113.5144462355907677, -24.66019654487200086, 8.947790411086106843 ) ) ;
#90104=CARTESIAN_POINT ( 'NONE',  ( -115.6228709571500559, -24.99156045073393173, 7.747789690856161648 ) ) ;
#90105=CARTESIAN_POINT ( 'NONE',  ( 11.36372850657041589, -19.49111573544105624, 11.49999999999999645 ) ) ;
#90106=EDGE_LOOP ( 'NONE', ( #55608, #69165, #53479, #10469 ) ) ;
#90107=CARTESIAN_POINT ( 'NONE',  ( -28.70433822602927876, -24.95898107482323169, 2.741470262984665229 ) ) ;
#90108=CARTESIAN_POINT ( 'NONE',  ( 19.14557405504459453, -10.84957060938160289, 11.49999999999998934 ) ) ;
#90110=CARTESIAN_POINT ( 'NONE',  ( -41.86995616089613748, -25.29087333980782404, 4.210709713361239004 ) ) ;
#90111=EDGE_LOOP ( 'NONE', ( #95152, #31823, #74108, #68719 ) ) ;
#90118=CARTESIAN_POINT ( 'NONE',  ( -126.5228709571500616, -24.64898659630368627, 1.056161002820834804 ) ) ;
#90119=CARTESIAN_POINT ( 'NONE',  ( -87.52287095715006160, -29.50247984919015209, -1.443849546365051806 ) ) ;
#90121=CARTESIAN_POINT ( 'NONE',  ( -8.611577853089924517, -18.50786853157798006, -1.500000000000002220 ) ) ;
#90122=ADVANCED_FACE ( 'NONE', ( #76651 ), #7153, .T. ) ;
#90123=ORIENTED_EDGE ( 'NONE', *, *, #6911, .F. ) ;
#90126=VECTOR ( 'NONE', #53144, 1000.000000000000114 ) ;
#90127=CARTESIAN_POINT ( 'NONE',  ( -105.5855877894006625, -24.92564183028979130, 1.928384488918251316 ) ) ;
#90128=FACE_OUTER_BOUND ( 'NONE', #32557, .T. ) ;
#90129=ADVANCED_FACE ( 'NONE', ( #15266 ), #81718, .T. ) ;
#90132=CARTESIAN_POINT ( 'NONE',  ( -59.56094173781918499, -25.21083105912962097, 3.409327675794633805 ) ) ;
#90134=CARTESIAN_POINT ( 'NONE',  ( 17.18838054715250152, -11.71887806637979779, 11.49999999999998934 ) ) ;
#90136=CARTESIAN_POINT ( 'NONE',  ( -101.6367431519704212, -23.48783264082477018, -1.443836473390089248 ) ) ;
#90139=CARTESIAN_POINT ( 'NONE',  ( -127.6228709571500275, -24.66019654487199730, 8.947790411086121054 ) ) ;
#90140=CARTESIAN_POINT ( 'NONE',  ( -128.5228709571500758, -23.48786465467242479, 11.44779295918253581 ) ) ;
#90144=CARTESIAN_POINT ( 'NONE',  ( -33.52287095715006160, -24.64965694238574656, 8.947790433994207149 ) ) ;
#90145=CARTESIAN_POINT ( 'NONE',  ( -118.7287200997191405, -25.23482084814633097, 3.690491797311988176 ) ) ;
#90146=AXIS2_PLACEMENT_3D ( 'NONE', #22887, #99025, #91417 ) ;
#90147=CARTESIAN_POINT ( 'NONE',  ( -80.62287095715007013, -25.00158670708909625, 2.256160236439165967 ) ) ;
#90148=CARTESIAN_POINT ( 'NONE',  ( -43.52203307092815265, -23.48786465467240347, 11.44779295918255180 ) ) ;
#90149=CARTESIAN_POINT ( 'NONE',  ( -4.315754209668272168, 21.71352930684897942, 11.49999999999999645 ) ) ;
#90152=LINE ( 'NONE', #23611, #61837 ) ;
#90153=CARTESIAN_POINT ( 'NONE',  ( -21.41681981171885951, -7.298096547245328303, 11.49999999999998934 ) ) ;
#90154=EDGE_CURVE ( 'NONE', #46797, #79998, #80178, .T. ) ;
#90155=CARTESIAN_POINT ( 'NONE',  ( -115.6284348552737811, -24.15602025860897584, 10.28564288303533836 ) ) ;
#90157=EDGE_LOOP ( 'NONE', ( #67270, #97724, #22492, #91638 ) ) ;
#90158=B_SPLINE_CURVE_WITH_KNOTS ( 'NONE', 3,
 ( #96097, #18461, #65171, #57546 ),
 .UNSPECIFIED., .F., .F.,
 ( 4, 4 ),
 ( 0.000000000000000000, 9.999999999998897304E-05 ),
 .UNSPECIFIED. ) ;
#90159=CARTESIAN_POINT ( 'NONE',  ( -80.85430032345135487, -25.31559690359951631, 5.016450530977278000 ) ) ;
#90160=ADVANCED_FACE ( 'NONE', ( #79668 ), #21790, .T. ) ;
#90164=CARTESIAN_POINT ( 'NONE',  ( -103.5228709571500758, -24.64965694238408034, 8.947790433994194714 ) ) ;
#90165=CARTESIAN_POINT ( 'NONE',  ( 20.80681148587913754, 8.022540738981085440, -1.500000000000002220 ) ) ;
#90166=CARTESIAN_POINT ( 'NONE',  ( -50.22356044790234364, -25.13941496013254095, 7.558302963627013149 ) ) ;
#90168=LINE ( 'NONE', #34889, #67603 ) ;
#90169=DIRECTION ( 'NONE',  ( 1.000000000000000000, 3.773278334444166432E-23, 8.201307841325785021E-29 ) ) ;
#90172=CARTESIAN_POINT ( 'NONE',  ( -84.62287095715004170, -24.65952944569304606, 1.056160979905699460 ) ) ;
#90174=CARTESIAN_POINT ( 'NONE',  ( -19.43040671759091609, -1.856541507571394467, -1.500000000000002220 ) ) ;
#90175=CARTESIAN_POINT ( 'NONE',  ( 14.05358622956002357, 16.19628355576825385, 11.49999999999998934 ) ) ;
#90176=FACE_OUTER_BOUND ( 'NONE', #37303, .T. ) ;
#90179=CARTESIAN_POINT ( 'NONE',  ( -5.953223121155255981, 22.05028593715628560, -1.500000000000002220 ) ) ;
#90182=CARTESIAN_POINT ( 'NONE',  ( -128.5228709571500758, -24.33832256527048798, 0.1851278514138663678 ) ) ;
#90183=CARTESIAN_POINT ( 'NONE',  ( 14.90458806734895703, -13.33898509196910886, 11.49999999999999645 ) ) ;
#90185=CARTESIAN_POINT ( 'NONE',  ( -74.54207935781894889, -24.51419770103157703, 9.386484678747164523 ) ) ;
#90186=CARTESIAN_POINT ( 'NONE',  ( -48.51406547070947539, -23.73766607897670866, -1.055555164236436028 ) ) ;
#90187=ORIENTED_EDGE ( 'NONE', *, *, #34564, .T. ) ;
#90188=CARTESIAN_POINT ( 'NONE',  ( -26.12160690352767389, -24.70321153058107910, 2.461338914291016255 ) ) ;
#90189=CARTESIAN_POINT ( 'NONE',  ( -65.52287095715006160, -23.48786465467241058, 11.44779295918254647 ) ) ;
#90190=CARTESIAN_POINT ( 'NONE',  ( 13.45394552336293614, 17.01807010946250287, -1.500000000000002220 ) ) ;
#90192=CARTESIAN_POINT ( 'NONE',  ( -19.51626497420292239, -0.3564122556526727048, -1.500000000000002220 ) ) ;
#90198=CARTESIAN_POINT ( 'NONE',  ( -65.55620429048339304, -23.47596703998600276, 11.44779298504227505 ) ) ;
#90199=CARTESIAN_POINT ( 'NONE',  ( 8.813945691637787405, 18.49579627399651471, 11.49999999999999645 ) ) ;
#90201=VECTOR ( 'NONE', #52398, 1000.000000000000114 ) ;
#90202=CARTESIAN_POINT ( 'NONE',  ( -84.62287095715005592, -29.50250243563736774, 8.947779886222141599 ) ) ;
#90203=VERTEX_POINT ( 'NONE', #66487 ) ;
#90204=CARTESIAN_POINT ( 'NONE',  ( -109.8274915671167093, -25.30623678762077233, 5.180956911978509716 ) ) ;
#90205=CARTESIAN_POINT ( 'NONE',  ( -86.52287095715006160, -24.64898659630367916, 1.056161002820827921 ) ) ;
#90206=AXIS2_PLACEMENT_3D ( 'NONE', #53095, #6901, #30231 ) ;
#90208=ADVANCED_FACE ( 'NONE', ( #43122 ), #12655, .T. ) ;
#90210=LINE ( 'NONE', #15078, #92145 ) ;
#90211=EDGE_CURVE ( 'NONE', #24849, #92377, #11807, .T. ) ;
#90214=VECTOR ( 'NONE', #62895, 1000.000000000000114 ) ;
#90215=ADVANCED_FACE ( 'NONE', ( #35995 ), #83161, .T. ) ;
#90216=CARTESIAN_POINT ( 'NONE',  ( -21.75560140871883164, 7.562747417745157463, 11.49999999999999645 ) ) ;
#90217=CARTESIAN_POINT ( 'NONE',  ( -22.52399778787742335, 3.408274809117095572, 11.49999999999998934 ) ) ;
#90218=LINE ( 'NONE', #13076, #74607 ) ;
#90221=CARTESIAN_POINT ( 'NONE',  ( -61.64687923781919920, -25.13069339737145214, 2.947789366383932297 ) ) ;
#90222=CARTESIAN_POINT ( 'NONE',  ( -115.5228709571500474, -24.63287334234179937, 0.9662140553045351909 ) ) ;
#90224=CARTESIAN_POINT ( 'NONE',  ( -104.2228709571500644, -23.47596703998600631, 11.44779298504227860 ) ) ;
#90225=CARTESIAN_POINT ( 'NONE',  ( -16.46405638241306946, -14.47283864684382237, -1.500000000000002220 ) ) ;
#90226=DIRECTION ( 'NONE',  ( 1.000000000000000000, 3.773278334444167608E-23, 8.201307833595939069E-29 ) ) ;
#90227=DIRECTION ( 'NONE',  ( 0.000000000000000000, -0.9999999999976377785, -2.173523156925979975E-06 ) ) ;
#90228=CARTESIAN_POINT ( 'NONE',  ( -71.20541289166536103, -25.30502758240210071, 4.885889971059796721 ) ) ;
#90229=CARTESIAN_POINT ( 'NONE',  ( -58.62366805386946567, -24.65952944569304606, 1.056160979905697461 ) ) ;
#90231=CARTESIAN_POINT ( 'NONE',  ( 18.81987132735423174, -8.002443037797982939, 11.49999999999998934 ) ) ;
#90234=ORIENTED_EDGE ( 'NONE', *, *, #43978, .F. ) ;
#90236=CARTESIAN_POINT ( 'NONE',  ( -13.44081803467414638, 18.71018530922267686, -1.500000000000002220 ) ) ;
#90237=CARTESIAN_POINT ( 'NONE',  ( -95.58953762381672448, -25.00158670708909625, 2.256160236439167299 ) ) ;
#90238=CARTESIAN_POINT ( 'NONE',  ( -2.107266074560359748, -20.09985696230311447, -1.500000000000002220 ) ) ;
#90241=CARTESIAN_POINT ( 'NONE',  ( -98.62287095715002749, -23.72773821059535848, 11.05748984161097326 ) ) ;
#90242=CARTESIAN_POINT ( 'NONE',  ( -41.73392779468957769, -25.31439885490801345, 4.813727054875380773 ) ) ;
#90243=EDGE_CURVE ( 'NONE', #84363, #62727, #3390, .T. ) ;
#90244=CARTESIAN_POINT ( 'NONE',  ( -118.6228709571500559, -29.50248528299804818, 1.056150453629045360 ) ) ;
#90245=CARTESIAN_POINT ( 'NONE',  ( -99.54653281135311715, -24.66019654487200086, 8.947790411086117501 ) ) ;
#90246=CARTESIAN_POINT ( 'NONE',  ( -15.65470850568805083, 14.63654280257262386, 11.49999999999999645 ) ) ;
#90247=VERTEX_POINT ( 'NONE', #66970 ) ;
#90248=LINE ( 'NONE', #76500, #59779 ) ;
#90249=ORIENTED_EDGE ( 'NONE', *, *, #99289, .T. ) ;
#90251=CARTESIAN_POINT ( 'NONE',  ( 11.91227609878784399, -18.80521639033699799, 11.49999999999998934 ) ) ;
#90252=CARTESIAN_POINT ( 'NONE',  ( 15.29587703590233971, -13.95322596517325664, 11.49999999999998934 ) ) ;
#90253=B_SPLINE_CURVE_WITH_KNOTS ( 'NONE', 3,
 ( #1147, #15853, #9245, #78247 ),
 .UNSPECIFIED., .F., .F.,
 ( 4, 4 ),
 ( 0.8811291927886271136, 0.8901356240607424253 ),
 .UNSPECIFIED. ) ;
#90254=ORIENTED_EDGE ( 'NONE', *, *, #14474, .T. ) ;
#90255=CARTESIAN_POINT ( 'NONE',  ( -28.60235993766668017, -23.80466053152675698, -0.6495505116914124244 ) ) ;
#90257=CARTESIAN_POINT ( 'NONE',  ( -74.62287095715005592, -29.50250786944525672, 11.44777988621623699 ) ) ;
#90259=CARTESIAN_POINT ( 'NONE',  ( 17.09260067683297635, -12.12037977771017871, -1.500000000000002220 ) ) ;
#90260=CARTESIAN_POINT ( 'NONE',  ( 6.672210613628693388, 20.84999943921648935, 11.49999999999999645 ) ) ;
#90261=CARTESIAN_POINT ( 'NONE',  ( -37.48483847649136891, -24.51419770103156637, 9.386484678747175181 ) ) ;
#90262=CARTESIAN_POINT ( 'NONE',  ( -11.40494320173684351, 19.43794304404440254, 11.49999999999998934 ) ) ;
#90264=CARTESIAN_POINT ( 'NONE',  ( 20.69369447470243628, -3.267675865747468489, -1.500000000000002220 ) ) ;
#90266=B_SPLINE_CURVE_WITH_KNOTS ( 'NONE', 3,
 ( #37400, #30776, #15042, #83556 ),
 .UNSPECIFIED., .F., .F.,
 ( 4, 4 ),
 ( 0.000000000000000000, 1.000000000000000000 ),
 .UNSPECIFIED. ) ;
#90267=CARTESIAN_POINT ( 'NONE',  ( -119.5222409990807506, -23.48786465467241769, 11.44779295918253759 ) ) ;
#90269=ORIENTED_EDGE ( 'NONE', *, *, #94259, .T. ) ;
#90271=ORIENTED_EDGE ( 'NONE', *, *, #72637, .F. ) ;
#90273=AXIS2_PLACEMENT_3D ( 'NONE', #43058, #3006, #26824 ) ;
#90274=CARTESIAN_POINT ( 'NONE',  ( -14.42888051209446409, 15.91495273949476363, -1.500000000000002220 ) ) ;
#90276=CARTESIAN_POINT ( 'NONE',  ( -121.5228709571500190, -24.66019654487199730, 8.947790411086119278 ) ) ;
#90279=CARTESIAN_POINT ( 'NONE',  ( 11.07546443054301655, -17.96822238807187233, 11.49999999999998934 ) ) ;
#90281=DIRECTION ( 'NONE',  ( -0.5658830507178048697, 0.000000000000000000, 0.8244855201338046058 ) ) ;
#90285=CARTESIAN_POINT ( 'NONE',  ( -37.52287095715006870, -23.47596703998600631, 11.44779298504229281 ) ) ;
#90286=CARTESIAN_POINT ( 'NONE',  ( -17.14978611337857473, 13.99085498846200437, -1.500000000000002220 ) ) ;
#90287=CARTESIAN_POINT ( 'NONE',  ( -108.8968792378191921, -25.14264220134206695, 6.986250900936221697 ) ) ;
#90289=CARTESIAN_POINT ( 'NONE',  ( -108.9606173779806682, -25.28716625322443790, 4.328991613801438376 ) ) ;
#90291=CARTESIAN_POINT ( 'NONE',  ( -97.52287095715011844, -24.33927499327856125, 9.819080762295813614 ) ) ;
#90292=CARTESIAN_POINT ( 'NONE',  ( 14.64286990871793392, 12.78475832571431070, -1.500000000000002220 ) ) ;
#90293=CARTESIAN_POINT ( 'NONE',  ( 18.88549913130557556, 9.949676122998861061, 11.49999999999998934 ) ) ;
#90295=CARTESIAN_POINT ( 'NONE',  ( -51.94775699965006766, -25.32724633150699489, 4.398074151685129607 ) ) ;
#90296=DIRECTION ( 'NONE',  ( 0.000000000000000000, -2.173523156925979552E-06, 0.9999999999976378895 ) ) ;
#90299=CARTESIAN_POINT ( 'NONE',  ( -15.94491270116497184, -16.04792668696150315, -1.500000000000002220 ) ) ;
#90301=CARTESIAN_POINT ( 'NONE',  ( -87.52287095715010423, -24.35013146730204170, 9.818937971375099494 ) ) ;
#90302=CARTESIAN_POINT ( 'NONE',  ( -104.6228709571500559, -24.64965695001468404, 8.947790433994178727 ) ) ;
#90303=CARTESIAN_POINT ( 'NONE',  ( -7.851535696030730982, 18.15458241006858131, 11.49999999999999645 ) ) ;
#90305=B_SPLINE_CURVE_WITH_KNOTS ( 'NONE', 3,
 ( #46288, #15323, #30051, #61027, #69121, #77217, #69634, #22429 ),
 .UNSPECIFIED., .F., .F.,
 ( 4, 2, 2, 4 ),
 ( -0.001240666984356056596, -0.0002401179793396612111, 0.0007604310256767346076, 0.002761529035709530365 ),
 .UNSPECIFIED. ) ;
#90306=CARTESIAN_POINT ( 'NONE',  ( -76.62287095715007013, -23.48783264082478084, -1.443836473390065489 ) ) ;
#90309=CARTESIAN_POINT ( 'NONE',  ( -29.81001385051325414, -25.26026941986502550, 4.645689688962429287 ) ) ;
#90310=CARTESIAN_POINT ( 'NONE',  ( -100.9506922656100727, -25.12268545600608860, 7.008856018889373374 ) ) ;
#90311=CARTESIAN_POINT ( 'NONE',  ( -19.46174652491427182, -9.421329337880418819, -1.500000000000002220 ) ) ;
#90314=CARTESIAN_POINT ( 'NONE',  ( -9.862393454161701101, 16.67994275214481092, -1.500000000000002220 ) ) ;
#90316=CARTESIAN_POINT ( 'NONE',  ( -40.62287095715004170, -24.99156045073392463, 7.747789690856161648 ) ) ;
#90317=CARTESIAN_POINT ( 'NONE',  ( -7.013475202606065828, -18.52788797337992222, 11.49999999999998934 ) ) ;
#90318=VERTEX_POINT ( 'NONE', #97400 ) ;
#90320=CARTESIAN_POINT ( 'NONE',  ( -17.45352675615719917, 10.31968153043333380, 11.49999999999999645 ) ) ;
#90321=CARTESIAN_POINT ( 'NONE',  ( -58.62287095715004881, -29.50247984919015209, -1.443849546365056913 ) ) ;
#90326=CARTESIAN_POINT ( 'NONE',  ( -99.52287095715006160, -23.48786465467241769, 11.44779295918254114 ) ) ;
#90329=CARTESIAN_POINT ( 'NONE',  ( -10.05502934987021391, 17.38067806581081598, -1.500000000000002220 ) ) ;
#90333=CARTESIAN_POINT ( 'NONE',  ( 22.28265747778879202, 5.072132558558076099, 11.49999999999999645 ) ) ;
#90334=CARTESIAN_POINT ( 'NONE',  ( -49.50841769935764347, -25.26258722004150670, 3.984447755610470487 ) ) ;
#90335=EDGE_CURVE ( 'NONE', #87641, #3446, #21752, .T. ) ;
#90336=CARTESIAN_POINT ( 'NONE',  ( -127.5228709571500900, -23.72747288104470798, -1.053458166803224572 ) ) ;
#90337=FACE_OUTER_BOUND ( 'NONE', #29575, .T. ) ;
#90338=B_SPLINE_CURVE_WITH_KNOTS ( 'NONE', 3,
 ( #69644, #14336, #76235, #45313, #92460, #46298 ),
 .UNSPECIFIED., .F., .F.,
 ( 4, 2, 4 ),
 ( 1.570755371634131319E-05, 0.001396183895866088404, 0.002776660238015835579 ),
 .UNSPECIFIED. ) ;
#90339=ADVANCED_FACE ( 'NONE', ( #59850 ), #30749, .T. ) ;
#90340=CARTESIAN_POINT ( 'NONE',  ( -71.52287095715007581, -24.64898659630528854, 1.056161002820824368 ) ) ;
#90341=VECTOR ( 'NONE', #79004, 1000.000000000000114 ) ;
#90343=CARTESIAN_POINT ( 'NONE',  ( -16.61153998044026991, -15.06042057022924929, 11.49999999999999645 ) ) ;
#90344=CARTESIAN_POINT ( 'NONE',  ( -74.62287095715005592, -24.64898659630367561, 1.056161002820824368 ) ) ;
#90346=VECTOR ( 'NONE', #39602, 1000.000000000000114 ) ;
#90347=CARTESIAN_POINT ( 'NONE',  ( -11.21218820807429140, -16.99972530465495169, 11.49999999999998934 ) ) ;
#90349=ADVANCED_FACE ( 'NONE', ( #29879 ), #7230, .T. ) ;
#90350=CARTESIAN_POINT ( 'NONE',  ( 2.177599385301639323, -22.86303409451243596, -1.500000000000002220 ) ) ;
#90351=LINE ( 'NONE', #45681, #97148 ) ;
#90352=VERTEX_POINT ( 'NONE', #92273 ) ;
#90353=CARTESIAN_POINT ( 'NONE',  ( -109.5228709571500758, -24.51283580621365488, 0.6167428607019762588 ) ) ;
#90354=CARTESIAN_POINT ( 'NONE',  ( -116.5228709571500616, -23.48786465467241769, 11.44779295918253759 ) ) ;
#90356=CARTESIAN_POINT ( 'NONE',  ( 9.297385241821217505, 19.04214385377821017, 11.49999999999999645 ) ) ;
#90357=ORIENTED_EDGE ( 'NONE', *, *, #63224, .F. ) ;
#90359=CARTESIAN_POINT ( 'NONE',  ( -18.13406196532287140, 12.77545654309102474, -1.500000000000002220 ) ) ;
#90360=CARTESIAN_POINT ( 'NONE',  ( 20.58124611042576646, 0.8182449333618511123, -1.500000000000002220 ) ) ;
#90362=ORIENTED_EDGE ( 'NONE', *, *, #84148, .T. ) ;
#90363=DIRECTION ( 'NONE',  ( 0.000000000000000000, 2.173523156925980399E-06, -0.9999999999976378895 ) ) ;
#90364=CARTESIAN_POINT ( 'NONE',  ( -39.11308345346323279, -25.25305377910670757, 3.767574040739871677 ) ) ;
#90365=ORIENTED_EDGE ( 'NONE', *, *, #90686, .T. ) ;
#90369=PLANE ( 'NONE',  #92397 ) ;
#90371=CARTESIAN_POINT ( 'NONE',  ( 10.28901978357889035, -18.02705789925236957, -1.500000000000002220 ) ) ;
#90372=CARTESIAN_POINT ( 'NONE',  ( 11.36066313177254905, -18.55813952095733654, 11.49999999999999645 ) ) ;
#90373=VERTEX_POINT ( 'NONE', #46116 ) ;
#90374=DIRECTION ( 'NONE',  ( 0.000000000000000000, -0.9999999999976377785, -2.173523156925979975E-06 ) ) ;
#90376=VECTOR ( 'NONE', #6272, 1000.000000000000114 ) ;
#90377=CARTESIAN_POINT ( 'NONE',  ( -115.5138003424739850, -24.92564183028979130, 1.928384488918252870 ) ) ;
#90378=CARTESIAN_POINT ( 'NONE',  ( -10.09097066620046235, 20.03973272787133553, -1.500000000000002220 ) ) ;
#90380=CARTESIAN_POINT ( 'NONE',  ( -102.5228709571500900, -23.72773821059536559, 11.05748984161097503 ) ) ;
#90383=CARTESIAN_POINT ( 'NONE',  ( -71.70421716572423065, -25.26843853055491351, 6.074178405081902099 ) ) ;
#90385=B_SPLINE_CURVE_WITH_KNOTS ( 'NONE', 3,
 ( #34707, #11367, #65186, #96595 ),
 .UNSPECIFIED., .F., .F.,
 ( 4, 4 ),
 ( 2.775557561562891351E-17, 0.0001000000000000167286 ),
 .UNSPECIFIED. ) ;
#90386=B_SPLINE_SURFACE_WITH_KNOTS ( 'NONE', 3, 3, ( 
 ( #58482, #81801, #83788, #29497 ),
 ( #43254, #82792, #20885, #66610 ),
 ( #13272, #44248, #52849, #52354 ),
 ( #89914, #51357, #74194, #75176 ),
 ( #59975, #58975, #5670, #36620 ),
 ( #98004, #4687, #35635, #59469 ),
 ( #97520, #67589, #12276, #19890 ) ),
 .UNSPECIFIED., .F., .F., .F.,
 ( 4, 3, 4 ),
 ( 4, 4 ),
 ( 0.0004766839783845967446, 0.1029713700210911909, 0.2054660560637977806 ),
 ( 0.1795396690725346300, 0.1806352329019877689 ),
 .UNSPECIFIED. ) ;
#90387=VERTEX_POINT ( 'NONE', #30881 ) ;
#90388=VERTEX_POINT ( 'NONE', #68945 ) ;
#90389=CARTESIAN_POINT ( 'NONE',  ( -108.5228709571500616, -24.65952944569304961, 1.056160979905704123 ) ) ;
#90391=ORIENTED_EDGE ( 'NONE', *, *, #78833, .T. ) ;
#90392=CARTESIAN_POINT ( 'NONE',  ( -15.93125441714207646, -14.09135727244061265, -1.500000000000002220 ) ) ;
#90396=CARTESIAN_POINT ( 'NONE',  ( 21.05697796394607835, 5.830696701215154043, 11.49999999999998934 ) ) ;
#90398=CARTESIAN_POINT ( 'NONE',  ( 13.52301212282245935, 18.22803923376396540, 11.49999999999998934 ) ) ;
#90399=CARTESIAN_POINT ( 'NONE',  ( -40.93315603532715130, -25.28892444152159769, 3.395436525629587088 ) ) ;
#90401=CARTESIAN_POINT ( 'NONE',  ( 12.42595048307055983, -18.10569578304522764, -1.500000000000002220 ) ) ;
#90402=CARTESIAN_POINT ( 'NONE',  ( -39.52287095715006870, -24.65952944569304606, 1.056160979905691910 ) ) ;
#90403=ORIENTED_EDGE ( 'NONE', *, *, #43275, .T. ) ;
#90405=VERTEX_POINT ( 'NONE', #53232 ) ;
#90406=CARTESIAN_POINT ( 'NONE',  ( -116.6228709571499991, -23.94994826722566117, -0.6494450866342701412 ) ) ;
#90407=CARTESIAN_POINT ( 'NONE',  ( -130.5728709571500588, -24.47917135695840685, 9.440663514584114679 ) ) ;
#90408=CARTESIAN_POINT ( 'NONE',  ( -10.27976737060564361, -22.47453952272712385, -0.4716817114508953246 ) ) ;
#90409=CARTESIAN_POINT ( 'NONE',  ( -8.014198274750887308, -19.69740135394370384, 11.49999999999998934 ) ) ;
#90411=CARTESIAN_POINT ( 'NONE',  ( -40.01839366089613748, -25.29500187561385260, 5.509688069775453556 ) ) ;
#90412=ADVANCED_FACE ( 'NONE', ( #7044 ), #60722, .T. ) ;
#90413=DIRECTION ( 'NONE',  ( 0.000000000000000000, 0.9999999999976377785, 2.173523156925979975E-06 ) ) ;
#90415=DIRECTION ( 'NONE',  ( 0.000000000000000000, -2.173523156925979552E-06, 0.9999999999976378895 ) ) ;
#90416=CARTESIAN_POINT ( 'NONE',  ( -117.5209649390443758, -23.73791477778912551, 11.05961554403169878 ) ) ;
#90418=CARTESIAN_POINT ( 'NONE',  ( -6.824658503225996320, 18.35159230250476270, 11.49999999999999645 ) ) ;
#90419=CARTESIAN_POINT ( 'NONE',  ( -114.6228709571500559, -29.50248528299804818, 1.056150453629043584 ) ) ;
#90420=VECTOR ( 'NONE', #72586, 1000.000000000000227 ) ;
#90421=CARTESIAN_POINT ( 'NONE',  ( -115.6228709571500559, -29.50247984919015209, -1.443849546365046699 ) ) ;
#90423=CARTESIAN_POINT ( 'NONE',  ( -88.60252819948608760, -23.48786465467241413, 11.44779295918254469 ) ) ;
#90424=EDGE_CURVE ( 'NONE', #44949, #66931, #62690, .T. ) ;
#90425=CARTESIAN_POINT ( 'NONE',  ( -100.5423878678571725, -25.03330743373828327, 7.561026521112214738 ) ) ;
#90427=CARTESIAN_POINT ( 'NONE',  ( -50.33541908643975660, -25.12321947555366819, 7.100310136161304797 ) ) ;
#90428=CARTESIAN_POINT ( 'NONE',  ( -5.312243195520525596, -18.98051080891723430, 11.49999999999998934 ) ) ;
#90430=B_SPLINE_CURVE_WITH_KNOTS ( 'NONE', 3,
 ( #10230, #2630, #3136, #18836, #49817, #57430 ),
 .UNSPECIFIED., .F., .F.,
 ( 4, 2, 4 ),
 ( 6.384118678615735980E-06, 0.001386860460828379755, 0.002767336802978144061 ),
 .UNSPECIFIED. ) ;
#90437=CARTESIAN_POINT ( 'NONE',  ( -84.58953762381671027, -23.48783264082479150, -1.443836473390065489 ) ) ;
#90439=CARTESIAN_POINT ( 'NONE',  ( -62.92287095715004597, -23.47593901973090169, -1.443836447538997536 ) ) ;
#90441=CARTESIAN_POINT ( 'NONE',  ( -99.62287095715004170, -23.73934037231757799, 11.05740245334328087 ) ) ;
#90443=CARTESIAN_POINT ( 'NONE',  ( 17.47191945374660094, 9.613082372698542599, -1.500000000000002220 ) ) ;
#90447=VERTEX_POINT ( 'NONE', #94275 ) ;
#90448=CARTESIAN_POINT ( 'NONE',  ( -101.7776484685884242, -25.26303730729093644, 3.986250639247583827 ) ) ;
#90452=LINE ( 'NONE', #66152, #12116 ) ;
#90453=CARTESIAN_POINT ( 'NONE',  ( -39.66516719614519815, -23.48783264082476308, -1.443836473390098352 ) ) ;
#90454=ADVANCED_FACE ( 'NONE', ( #49128 ), #71961, .T. ) ;
#90455=CARTESIAN_POINT ( 'NONE',  ( -119.6228709571500559, -23.94994826722566117, -0.6494450866342695861 ) ) ;
#90456=CARTESIAN_POINT ( 'NONE',  ( -51.66173670239771099, -25.31574316003434078, 4.265171533202613219 ) ) ;
#90457=EDGE_LOOP ( 'NONE', ( #97475, #28240, #18109, #74166 ) ) ;
#90458=B_SPLINE_SURFACE_WITH_KNOTS ( 'NONE', 3, 1, ( 
 ( #5393, #12503 ),
 ( #67812, #27736 ),
 ( #66318, #43468 ),
 ( #97739, #51576 ),
 ( #82509, #36347 ),
 ( #67303, #98226 ),
 ( #61691, #61198 ),
 ( #68794, #46450 ),
 ( #69791, #76384 ),
 ( #53583, #75891 ),
 ( #91123, #21596 ),
 ( #269, #7880 ),
 ( #52571, #30723 ),
 ( #44966, #76873 ),
 ( #83504, #60693 ),
 ( #13989, #31216 ),
 ( #45468, #100204 ),
 ( #6393, #68293 ),
 ( #92610, #92117 ),
 ( #84508, #69288 ),
 ( #23090, #8382 ),
 ( #29726, #91615 ),
 ( #62187, #39328 ),
 ( #22587, #70291 ),
 ( #37352, #99223 ),
 ( #93112, #6885 ),
 ( #22095, #54562 ) ),
 .UNSPECIFIED., .F., .F., .F.,
 ( 4, 1, 1, 1, 1, 1, 1, 1, 1, 1, 1, 1, 1, 1, 1, 1, 1, 1, 1, 1, 1, 1, 1, 1, 4 ),
 ( 2, 2 ),
 ( 0.000000000000000000, 0.03378714634699071101, 0.06662165772429405608, 0.09928487809597190406, 0.1313611650426508015, 0.1635851875953426293, 0.1961039269870683555, 0.2289022543238164731, 0.2621580559050077919, 0.2959912222583166441, 0.3302178457248000631, 0.3650598258919540706, 0.4009507373401078323, 0.4376203820767375907, 0.4757075294370922136, 0.5153806916250485148, 0.5564135414931642432, 0.5997648298727311644, 0.6464241555840872788, 0.6964314445175667778, 0.7497815178015574400, 0.8065733069755323115, 0.8674355315653993204, 0.9318867532508741114, 1.000000000000000000 ),
 ( 0.000000000000000000, 1.000000000000000000 ),
 .UNSPECIFIED. ) ;
#90460=CARTESIAN_POINT ( 'NONE',  ( -127.5903464641895937, -23.73766607897670511, -1.055555164236447130 ) ) ;
#90462=CARTESIAN_POINT ( 'NONE',  ( 19.74221769882431587, -4.499994434135383692, -1.500000000000002220 ) ) ;
#90463=CARTESIAN_POINT ( 'NONE',  ( -70.27422298781921484, -25.31465149953924865, 4.851635142449610250 ) ) ;
#90466=AXIS2_PLACEMENT_3D ( 'NONE', #23668, #55649, #30285 ) ;
#90468=CARTESIAN_POINT ( 'NONE',  ( -109.6228709571501128, -24.33832256526969218, 0.1851278514119941987 ) ) ;
#90469=B_SPLINE_CURVE_WITH_KNOTS ( 'NONE', 3,
 ( #42305, #4217, #87956, #33666, #3727, #42790 ),
 .UNSPECIFIED., .F., .F.,
 ( 4, 2, 4 ),
 ( 6.384118678610730015E-06, 0.001386860460828374768, 0.002767336802978138856 ),
 .UNSPECIFIED. ) ;
#90470=ORIENTED_EDGE ( 'NONE', *, *, #51036, .F. ) ;
#90472=CARTESIAN_POINT ( 'NONE',  ( -105.5562042904833930, -25.00158670708909980, 2.256160236439166411 ) ) ;
#90473=CARTESIAN_POINT ( 'NONE',  ( 3.315226082619958881, 19.80964767386612380, -1.500000000000002220 ) ) ;
#90474=CARTESIAN_POINT ( 'NONE',  ( 11.23609023086081038, -17.74952302366565604, 11.49999999999999645 ) ) ;
#90476=CARTESIAN_POINT ( 'NONE',  ( -70.49783793440687418, -24.52399227489127043, 9.353111116836524630 ) ) ;
#90477=CARTESIAN_POINT ( 'NONE',  ( -12.21066354923914865, 18.40238043084326591, 11.49999999999998934 ) ) ;
#90478=CARTESIAN_POINT ( 'NONE',  ( 17.35315496411208613, -10.91789592880838811, 11.49999999999998934 ) ) ;
#90479=CARTESIAN_POINT ( 'NONE',  ( -46.92287095715006018, -23.47596703998600276, 11.44779298504227683 ) ) ;
#90480=CARTESIAN_POINT ( 'NONE',  ( -70.62287095715004170, -23.48783264082478084, -1.443836473390067265 ) ) ;
#90481=DIRECTION ( 'NONE',  ( 1.000000000000000000, 3.773278334444166432E-23, 8.201307841325785021E-29 ) ) ;
#90482=ORIENTED_EDGE ( 'NONE', *, *, #5463, .F. ) ;
#90483=CARTESIAN_POINT ( 'NONE',  ( -41.46611000704998418, -29.50249209050311094, 4.188164501617994695 ) ) ;
#90484=B_SPLINE_CURVE_WITH_KNOTS ( 'NONE', 3,
 ( #83155, #53227, #13639, #75535 ),
 .UNSPECIFIED., .F., .F.,
 ( 4, 4 ),
 ( 1.387778780781445521E-17, 0.0004038461538461296518 ),
 .UNSPECIFIED. ) ;
#90488=CARTESIAN_POINT ( 'NONE',  ( -83.58953762381673869, -24.65952944569304606, 1.056160979905698794 ) ) ;
#90489=DIRECTION ( 'NONE',  ( -3.773278334453079618E-23, 0.9999999999976377785, 2.173523156925979975E-06 ) ) ;
#90490=CARTESIAN_POINT ( 'NONE',  ( -44.52287095715006160, -23.48786465467241058, 11.44779295918255180 ) ) ;
#90491=CARTESIAN_POINT ( 'NONE',  ( -17.20787902393383462, -11.26661214947554157, -1.500000000000002220 ) ) ;
#90492=CARTESIAN_POINT ( 'NONE',  ( 19.31049906410359895, -9.575588319827552652, 11.49999999999999645 ) ) ;
#90493=ORIENTED_EDGE ( 'NONE', *, *, #3463, .T. ) ;
#90494=CARTESIAN_POINT ( 'NONE',  ( -99.64934318012689118, -25.30535455722350591, 4.927356316503054501 ) ) ;
#90496=CARTESIAN_POINT ( 'NONE',  ( 21.86734719908870872, 4.625976558377421277, 11.49999999999998934 ) ) ;
#90497=CARTESIAN_POINT ( 'NONE',  ( -124.6228709571500417, -24.65952944569304606, 1.056160979905705011 ) ) ;
#90498=LINE ( 'NONE', #45824, #59422 ) ;
#90500=CARTESIAN_POINT ( 'NONE',  ( -94.52287095715006160, -24.65952944569304961, 1.056160979905700570 ) ) ;
#90502=CARTESIAN_POINT ( 'NONE',  ( -13.97254113366623152, 15.51630364309664856, -1.500000000000002220 ) ) ;
#90504=CARTESIAN_POINT ( 'NONE',  ( -67.58020753937425695, -24.66019654487199730, 8.947790411086115725 ) ) ;
#90505=EDGE_LOOP ( 'NONE', ( #10128, #62640, #27721, #95579 ) ) ;
#90507=ADVANCED_FACE ( 'NONE', ( #9042 ), #59892, .T. ) ;
#90508=CARTESIAN_POINT ( 'NONE',  ( -100.6305594176849070, -24.40133493613050319, 9.663955038902802386 ) ) ;
#90509=CARTESIAN_POINT ( 'NONE',  ( 16.66693084842116335, 13.01107939256401913, -1.500000000000002220 ) ) ;
#90510=ORIENTED_EDGE ( 'NONE', *, *, #55909, .T. ) ;
#90511=CARTESIAN_POINT ( 'NONE',  ( -60.62287095715004881, -24.99156045073392463, 7.747789690856161648 ) ) ;
#90514=CARTESIAN_POINT ( 'NONE',  ( -76.55419120562295632, -23.96169478059713143, 10.65365249895718058 ) ) ;
#90515=CARTESIAN_POINT ( 'NONE',  ( -40.52287095715005449, -24.99156044556202261, 7.747789690856173195 ) ) ;
#90516=CARTESIAN_POINT ( 'NONE',  ( -21.04499429308205549, 5.405531755741471045, -1.500000000000002220 ) ) ;
#90517=CARTESIAN_POINT ( 'NONE',  ( -71.70379718938951896, -25.31639723079672066, 6.052014632951667750 ) ) ;
#90518=CARTESIAN_POINT ( 'NONE',  ( 18.98964132805693694, -11.70494588174365092, 11.49999999999999645 ) ) ;
#90522=PLANE ( 'NONE',  #248 ) ;
#90523=ORIENTED_EDGE ( 'NONE', *, *, #13692, .F. ) ;
#90524=ORIENTED_EDGE ( 'NONE', *, *, #9322, .T. ) ;
#90526=CARTESIAN_POINT ( 'NONE',  ( -56.62287095715008434, -23.47596703998600276, 11.44779298504227683 ) ) ;
#90529=DIRECTION ( 'NONE',  ( 0.9116753070387548785, -8.931253266735290907E-07, 0.4109113463205835703 ) ) ;
#90531=CARTESIAN_POINT ( 'NONE',  ( -19.35591191756920892, -0.7100623379298715010, 11.49999999999998934 ) ) ;
#90532=CARTESIAN_POINT ( 'NONE',  ( -31.52287095715006160, -24.66019654487198665, 8.947790411086131712 ) ) ;
#90533=ORIENTED_EDGE ( 'NONE', *, *, #83908, .F. ) ;
#90535=CARTESIAN_POINT ( 'NONE',  ( -13.40542139710017899, 13.98966777563825481, 11.49999999999999645 ) ) ;
#90543=EDGE_CURVE ( 'NONE', #78575, #11988, #33559, .T. ) ;
#90544=CARTESIAN_POINT ( 'NONE',  ( -36.52287095715009002, -24.66019654487199730, 8.947790411086124607 ) ) ;
#90545=CARTESIAN_POINT ( 'NONE',  ( 0.6594449095415070294, 19.62168050102039629, -1.500000000000002220 ) ) ;
#90548=ADVANCED_FACE ( 'NONE', ( #67337 ), #43004, .T. ) ;
#90549=CARTESIAN_POINT ( 'NONE',  ( 21.55061338234859392, -0.003183148592148328428, 11.49999999999998934 ) ) ;
#90550=AXIS2_PLACEMENT_3D ( 'NONE', #28805, #52149, #83076 ) ;
#90554=CARTESIAN_POINT ( 'NONE',  ( -100.0747864355570158, -25.18439346793923050, 3.344773611727388740 ) ) ;
#90555=CARTESIAN_POINT ( 'NONE',  ( 22.51966570110743149, 4.691836548664650053, -1.500000000000002220 ) ) ;
#90558=CARTESIAN_POINT ( 'NONE',  ( -44.62287095715004881, -24.66019654487198665, 8.947790411086135265 ) ) ;
#90559=CARTESIAN_POINT ( 'NONE',  ( -19.98115086844608612, 2.773124471107000666, 11.49999999999999645 ) ) ;
#90560=CARTESIAN_POINT ( 'NONE',  ( -71.22287095715005023, -23.47593901973090169, -1.443836447538997536 ) ) ;
#90561=CARTESIAN_POINT ( 'NONE',  ( -32.55272256901955075, -23.96169478059712787, 10.65365249895719124 ) ) ;
#90565=CARTESIAN_POINT ( 'NONE',  ( -111.2787752023839971, -25.18425713224470996, 3.894639490442704410 ) ) ;
#90566=CARTESIAN_POINT ( 'NONE',  ( -19.84341114293531305, -1.032944114202840824, 11.49999999999998934 ) ) ;
#90568=CARTESIAN_POINT ( 'NONE',  ( -99.62287095715005592, -29.50250786944525672, 11.44777988621623166 ) ) ;
#90569=CARTESIAN_POINT ( 'NONE',  ( -19.30086548479123465, -4.275078920326023990, -1.500000000000002220 ) ) ;
#90571=B_SPLINE_CURVE_WITH_KNOTS ( 'NONE', 3,
 ( #53798, #91343, #36555, #21818 ),
 .UNSPECIFIED., .F., .F.,
 ( 4, 4 ),
 ( 0.000000000000000000, 9.999999999999592548E-05 ),
 .UNSPECIFIED. ) ;
#90573=LINE ( 'NONE', #60149, #32944 ) ;
#90574=CARTESIAN_POINT ( 'NONE',  ( 18.79598114143782084, -8.675585332008726169, 11.49999999999999645 ) ) ;
#90577=CARTESIAN_POINT ( 'NONE',  ( -97.58953762381672448, -24.64965694238407323, 8.947790433994651238 ) ) ;
#90578=CARTESIAN_POINT ( 'NONE',  ( -49.52475239181693212, -25.31439355338475394, 5.557100884789670125 ) ) ;
#90579=AXIS2_PLACEMENT_3D ( 'NONE', #91175, #14041, #37895 ) ;
#90580=CARTESIAN_POINT ( 'NONE',  ( -14.94938274637043207, -17.11189489004485864, 11.49999999999999645 ) ) ;
#90581=ORIENTED_EDGE ( 'NONE', *, *, #38839, .F. ) ;
#90585=FACE_OUTER_BOUND ( 'NONE', #83861, .T. ) ;
#90588=EDGE_LOOP ( 'NONE', ( #66820, #9494, #31130, #18327 ) ) ;
#90590=ORIENTED_EDGE ( 'NONE', *, *, #25418, .F. ) ;
#90592=CARTESIAN_POINT ( 'NONE',  ( -14.01358469492184966, -18.07645309290061064, -1.500000000000002220 ) ) ;
#90593=CARTESIAN_POINT ( 'NONE',  ( -29.64367331884317025, -24.07992180899756107, -0.2315648265717072385 ) ) ;
#90594=ADVANCED_FACE ( 'NONE', ( #57735 ), #43502, .T. ) ;
#90595=CARTESIAN_POINT ( 'NONE',  ( 20.55510029441247610, -6.647428040031946317, -1.500000000000002220 ) ) ;
#90598=CARTESIAN_POINT ( 'NONE',  ( -13.16310354753345990, -18.33534949228788236, 11.49999999999999645 ) ) ;
#90600=CARTESIAN_POINT ( 'NONE',  ( -70.00627666057835086, -25.31612425288418322, 4.873906333287980175 ) ) ;
#90601=CARTESIAN_POINT ( 'NONE',  ( 14.26656746985186608, 16.74056184347216458, 11.49999999999998934 ) ) ;
#90602=CARTESIAN_POINT ( 'NONE',  ( -105.5120787285895148, -24.52399227489126687, 9.353111116836517525 ) ) ;
#90603=CARTESIAN_POINT ( 'NONE',  ( -40.99321688279000853, -25.10925790275778624, 2.933756721058497163 ) ) ;
#90605=EDGE_CURVE ( 'NONE', #94223, #27910, #35879, .T. ) ;
#90607=CARTESIAN_POINT ( 'NONE',  ( -90.62931513133528938, -24.63419186844611275, 9.035850630976923981 ) ) ;
#90609=CARTESIAN_POINT ( 'NONE',  ( -111.6228709571500559, -29.50247984919015209, -1.443849546365048253 ) ) ;
#90611=ORIENTED_EDGE ( 'NONE', *, *, #45542, .F. ) ;
#90612=AXIS2_PLACEMENT_3D ( 'NONE', #14327, #13330, #75237 ) ;
#90613=ORIENTED_EDGE ( 'NONE', *, *, #76134, .F. ) ;
#90615=CARTESIAN_POINT ( 'NONE',  ( -104.5228709571501184, -24.51283580621365132, 0.6167428607019820319 ) ) ;
#90616=CARTESIAN_POINT ( 'NONE',  ( -57.58748390918375293, -24.34968618360933590, 0.1864209137778796155 ) ) ;
#90617=CARTESIAN_POINT ( 'NONE',  ( 4.102729645046709450, 19.96921287702725323, -1.500000000000002220 ) ) ;
#90618=ORIENTED_EDGE ( 'NONE', *, *, #37346, .T. ) ;
#90619=CARTESIAN_POINT ( 'NONE',  ( -93.52287095715006160, -24.64965694238407323, 8.947790433994196491 ) ) ;
#90620=VECTOR ( 'NONE', #28978, 1000.000000000000114 ) ;
#90621=CARTESIAN_POINT ( 'NONE',  ( -30.61333094834724733, -24.36247485673954927, 0.01136689895587368430 ) ) ;
#90627=CARTESIAN_POINT ( 'NONE',  ( -60.95156673781919210, -25.21083105912962452, 3.409327675794633361 ) ) ;
#90628=VECTOR ( 'NONE', #98945, 1000.000000000000114 ) ;
#90629=CARTESIAN_POINT ( 'NONE',  ( -11.07951500695464553, -17.62175104703424466, -1.500000000000002220 ) ) ;
#90634=CARTESIAN_POINT ( 'NONE',  ( -56.52287095715006870, -23.47596703998600631, 11.44779298504228926 ) ) ;
#90635=ORIENTED_EDGE ( 'NONE', *, *, #84601, .F. ) ;
#90636=ORIENTED_EDGE ( 'NONE', *, *, #29430, .F. ) ;
#90639=CARTESIAN_POINT ( 'NONE',  ( -49.52287095715006160, -29.50248528299804818, 1.056150453629033370 ) ) ;
#90640=CARTESIAN_POINT ( 'NONE',  ( -70.46019744876114999, -25.31201591126554717, 5.316127909876582791 ) ) ;
#90641=CARTESIAN_POINT ( 'NONE',  ( -21.04927197579530329, -6.814310187297170529, 11.49999999999999645 ) ) ;
#90643=DIRECTION ( 'NONE',  ( -3.773278334453079618E-23, 0.9999999999976377785, 2.173523156925979975E-06 ) ) ;
#90644=CARTESIAN_POINT ( 'NONE',  ( 21.16457415087624128, -7.944649954575952577, -1.500000000000002220 ) ) ;
#90645=CARTESIAN_POINT ( 'NONE',  ( -46.52287095715005449, -23.96177878511308634, 10.65340807706331283 ) ) ;
#90650=ADVANCED_FACE ( 'NONE', ( #87994 ), #95599, .T. ) ;
#90651=CARTESIAN_POINT ( 'NONE',  ( -16.19606052442943067, -11.93128464602566474, 11.49999999999998934 ) ) ;
#90654=ORIENTED_EDGE ( 'NONE', *, *, #96315, .F. ) ;
#90655=EDGE_CURVE ( 'NONE', #50270, #20514, #63970, .T. ) ;
#90656=CARTESIAN_POINT ( 'NONE',  ( -107.6228709571500701, -24.64898659630368272, 1.056161002820831474 ) ) ;
#90657=CARTESIAN_POINT ( 'NONE',  ( -22.23078454666273274, -1.437644496696519170, -1.500000000000002220 ) ) ;
#90661=CARTESIAN_POINT ( 'NONE',  ( -110.5562042904833930, -23.48786465467242479, 11.44779295918253936 ) ) ;
#90662=FACE_OUTER_BOUND ( 'NONE', #77726, .T. ) ;
#90663=CARTESIAN_POINT ( 'NONE',  ( -25.85456927314744391, -24.76652822093846140, 2.947631189768983528 ) ) ;
#90664=ADVANCED_FACE ( 'NONE', ( #9355 ), #96107, .T. ) ;
#90667=CARTESIAN_POINT ( 'NONE',  ( -44.52287095715006160, -23.47596703998600631, 11.44779298504229281 ) ) ;
#90668=CARTESIAN_POINT ( 'NONE',  ( -13.79594968651775666, -13.80015156857029268, -1.500000000000002220 ) ) ;
#90669=EDGE_CURVE ( 'NONE', #72641, #50584, #54247, .T. ) ;
#90670=CARTESIAN_POINT ( 'NONE',  ( -19.33005188562793819, 9.364626179424670127, 11.49999999999998934 ) ) ;
#90671=CARTESIAN_POINT ( 'NONE',  ( -25.68905881183481199, -24.57999888590886073, 3.430378900168168599 ) ) ;
#90672=DIRECTION ( 'NONE',  ( 1.000000000000000000, 3.773278334444167608E-23, 8.201307833595939069E-29 ) ) ;
#90675=CARTESIAN_POINT ( 'NONE',  ( 10.87194125936840194, 20.03610521102953257, -1.500000000000002220 ) ) ;
#90677=CARTESIAN_POINT ( 'NONE',  ( -39.52287095715006870, -23.47593901973090524, -1.443836447538997092 ) ) ;
#90678=CARTESIAN_POINT ( 'NONE',  ( -108.5228709571500616, -24.65952944569304961, 1.056160979905704123 ) ) ;
#90679=CARTESIAN_POINT ( 'NONE',  ( -3.050325703546597822, 19.74810961616558913, 11.49999999999999645 ) ) ;
#90680=DIRECTION ( 'NONE',  ( -3.773278334444167608E-23, 1.000000000000000000, 0.000000000000000000 ) ) ;
#90682=CARTESIAN_POINT ( 'NONE',  ( -111.6228709571500559, -29.50250243563736774, 8.947779886222136270 ) ) ;
#90685=CARTESIAN_POINT ( 'NONE',  ( -56.92287095715008860, -23.47593901973090524, -1.443836447538998202 ) ) ;
#90686=EDGE_CURVE ( 'NONE', #34994, #63074, #80878, .T. ) ;
#90687=CARTESIAN_POINT ( 'NONE',  ( -93.52287095715006160, -29.50250243563736774, 8.947779886222139822 ) ) ;
#90688=CARTESIAN_POINT ( 'NONE',  ( 18.07971092720299922, 12.08445254275838465, -1.500000000000002220 ) ) ;
#90691=CARTESIAN_POINT ( 'NONE',  ( -3.586273028688536257, -19.27814873881845514, -1.500000000000002220 ) ) ;
#90698=CARTESIAN_POINT ( 'NONE',  ( -91.62357784265581984, -24.66019654487199730, 8.947790411086115725 ) ) ;
#90700=CARTESIAN_POINT ( 'NONE',  ( -3.437008290023895185, 20.19323497536227663, 11.49999999999999645 ) ) ;
#90704=AXIS2_PLACEMENT_3D ( 'NONE', #82893, #12879, #49983 ) ;
#90705=ORIENTED_EDGE ( 'NONE', *, *, #52540, .F. ) ;
#90709=CARTESIAN_POINT ( 'NONE',  ( -110.9909297185884327, -25.15277794460069671, 6.986250878905948980 ) ) ;
#90710=ORIENTED_EDGE ( 'NONE', *, *, #29663, .F. ) ;
#90713=CARTESIAN_POINT ( 'NONE',  ( -3.733506833432379768, 22.73668382284982314, 11.49999999999999645 ) ) ;
#90714=B_SPLINE_CURVE_WITH_KNOTS ( 'NONE', 3,
 ( #72128, #17319, #1608, #54894 ),
 .UNSPECIFIED., .F., .F.,
 ( 4, 4 ),
 ( 0.000000000000000000, 9.999999999998897304E-05 ),
 .UNSPECIFIED. ) ;
#90715=CARTESIAN_POINT ( 'NONE',  ( -4.374245501123523283, 22.36648047097513725, -1.500000000000002220 ) ) ;
#90716=CARTESIAN_POINT ( 'NONE',  ( -110.5947687508519692, -23.85049219812686516, 10.88485053497526955 ) ) ;
#90718=CARTESIAN_POINT ( 'NONE',  ( -50.29954090288276802, -25.19533727061342177, 3.296115780377149029 ) ) ;
#90720=B_SPLINE_CURVE_WITH_KNOTS ( 'NONE', 3,
 ( #79647, #33479, #25870, #13127 ),
 .UNSPECIFIED., .F., .F.,
 ( 4, 4 ),
 ( 0.000000000000000000, 9.999999999999592548E-05 ),
 .UNSPECIFIED. ) ;
#90721=CARTESIAN_POINT ( 'NONE',  ( -99.37735140507533060, -25.31582232917384800, 5.086082719468676849 ) ) ;
#90722=ADVANCED_FACE ( 'NONE', ( #34704 ), #33197, .T. ) ;
#90723=CARTESIAN_POINT ( 'NONE',  ( 21.14253370195585546, 5.708146584608840612, -1.500000000000002220 ) ) ;
#90725=CARTESIAN_POINT ( 'NONE',  ( -87.63525289881717129, -23.96169478059713498, 10.65365249895718058 ) ) ;
#90726=CARTESIAN_POINT ( 'NONE',  ( -33.52287095715007581, -24.51387760970725083, 9.387446482453428942 ) ) ;
#90728=LINE ( 'NONE', #21694, #88978 ) ;
#90731=CARTESIAN_POINT ( 'NONE',  ( 17.75789855128238770, 10.12834119215567164, 11.49999999999998934 ) ) ;
#90732=VERTEX_POINT ( 'NONE', #79366 ) ;
#90734=ORIENTED_EDGE ( 'NONE', *, *, #14481, .F. ) ;
#90735=ORIENTED_EDGE ( 'NONE', *, *, #70845, .F. ) ;
#90736=EDGE_CURVE ( 'NONE', #37215, #62489, #40810, .T. ) ;
#90737=CARTESIAN_POINT ( 'NONE',  ( 22.18053613645642841, 6.281410551025238043, 11.49999999999998934 ) ) ;
#90738=CARTESIAN_POINT ( 'NONE',  ( -61.53887241091420179, -24.51314013834316086, 0.6176544820404138436 ) ) ;
#90739=CARTESIAN_POINT ( 'NONE',  ( 15.69265952521009488, -12.80212094623039576, -1.500000000000002220 ) ) ;
#90740=VERTEX_POINT ( 'NONE', #71771 ) ;
#90741=CARTESIAN_POINT ( 'NONE',  ( -90.58953762381671027, -25.00182538069145366, 7.747789668545099317 ) ) ;
#90742=CARTESIAN_POINT ( 'NONE',  ( -41.18093725576135711, -25.30970379484010735, 5.386210342106713789 ) ) ;
#90743=CARTESIAN_POINT ( 'NONE',  ( -95.58789998751944950, -24.63355581998386157, 0.9682620441943944334 ) ) ;
#90745=CARTESIAN_POINT ( 'NONE',  ( 17.68986881342592454, -12.14045624799103962, 11.49999999999999645 ) ) ;
#90746=VERTEX_POINT ( 'NONE', #64179 ) ;
#90747=CARTESIAN_POINT ( 'NONE',  ( -100.5895376238167245, -23.47593901973091235, -1.443836447539001089 ) ) ;
#90749=CARTESIAN_POINT ( 'NONE',  ( 16.32338804990218151, -12.73490195939593406, -1.500000000000002220 ) ) ;
#90752=CARTESIAN_POINT ( 'NONE',  ( -113.6228709571500559, -24.65952944569304961, 1.056160979905706565 ) ) ;
#90753=ORIENTED_EDGE ( 'NONE', *, *, #98592, .F. ) ;
#90757=CARTESIAN_POINT ( 'NONE',  ( -19.40599490818632233, 7.965113791304038848, -1.500000000000002220 ) ) ;
#90758=CARTESIAN_POINT ( 'NONE',  ( -13.73438224071023761, 17.16576579689093762, 11.49999999999999645 ) ) ;
#90759=CARTESIAN_POINT ( 'NONE',  ( -89.62358331694552760, -24.66019654487199730, 8.947790411086115725 ) ) ;
#90760=CARTESIAN_POINT ( 'NONE',  ( -5.199590022849982063, -21.90925200621149571, 11.49999999999998934 ) ) ;
#90762=CARTESIAN_POINT ( 'NONE',  ( 5.724939850241691275, 20.19279902153374096, -1.500000000000002220 ) ) ;
#90764=CARTESIAN_POINT ( 'NONE',  ( -72.62287095715005592, -24.64898659630367916, 1.056161002820824368 ) ) ;
#90766=ORIENTED_EDGE ( 'NONE', *, *, #65035, .T. ) ;
#90768=B_SPLINE_CURVE_WITH_KNOTS ( 'NONE', 3,
 ( #21558, #84963, #99671, #23553, #45426, #52531 ),
 .UNSPECIFIED., .F., .F.,
 ( 4, 2, 4 ),
 ( 0.000000000000000000, 0.001380901958385383774, 0.002761803916770767548 ),
 .UNSPECIFIED. ) ;
#90774=CARTESIAN_POINT ( 'NONE',  ( 14.45597713831175035, -15.85640774750547344, -1.500000000000002220 ) ) ;
#90776=LINE ( 'NONE', #43608, #32693 ) ;
#90778=CARTESIAN_POINT ( 'NONE',  ( -9.620199658202244208, 18.81650055922726494, 11.49999999999998934 ) ) ;
#90779=CARTESIAN_POINT ( 'NONE',  ( -93.62287095715004170, -23.48783264082478794, -1.443836473390063713 ) ) ;
#90780=EDGE_CURVE ( 'NONE', #85400, #86130, #11618, .T. ) ;
#90781=CARTESIAN_POINT ( 'NONE',  ( -64.58769910004320991, -24.34968618360933590, 0.1864209137778785330 ) ) ;
#90783=CARTESIAN_POINT ( 'NONE',  ( -54.52287095715006870, -29.50250243563736774, 8.947779886222146928 ) ) ;
#90784=CARTESIAN_POINT ( 'NONE',  ( -99.12380231474227799, -25.26431306044052150, 4.001575155705512366 ) ) ;
#90785=CARTESIAN_POINT ( 'NONE',  ( -7.320055889550622474, -20.87099576385019972, -1.500000000000002220 ) ) ;
#90786=EDGE_CURVE ( 'NONE', #60457, #8399, #58058, .T. ) ;
#90787=CARTESIAN_POINT ( 'NONE',  ( -30.49308942697465952, -23.47593901973084485, -1.443836476861628970 ) ) ;
#90789=CARTESIAN_POINT ( 'NONE',  ( -56.52287095715007581, -24.33927499327853994, 9.819080762295817166 ) ) ;
#90790=CARTESIAN_POINT ( 'NONE',  ( -69.52287095715006160, -23.47593901973090169, -1.443836447538996870 ) ) ;
#90792=EDGE_CURVE ( 'NONE', #15522, #87638, #55315, .T. ) ;
#90793=CARTESIAN_POINT ( 'NONE',  ( -100.5540451804232589, -24.15503026093913874, -0.2815557561904538653 ) ) ;
#90794=CARTESIAN_POINT ( 'NONE',  ( -18.32239908988104204, -6.426282940459683068, 11.49999999999998934 ) ) ;
#90795=CARTESIAN_POINT ( 'NONE',  ( -2.881439591185620319, 21.19155266312798958, 11.49999999999998934 ) ) ;
#90796=CARTESIAN_POINT ( 'NONE',  ( -66.58953762381672448, -23.48783264082478439, -1.443836473390067487 ) ) ;
#90797=DIRECTION ( 'NONE',  ( -3.773278334453079618E-23, 0.9999999999976377785, 2.173523156925979975E-06 ) ) ;
#90798=CARTESIAN_POINT ( 'NONE',  ( -123.5228709571500616, -23.72747288104470442, -1.053458166803224794 ) ) ;
#90799=CARTESIAN_POINT ( 'NONE',  ( -60.62287095715005592, -23.48786465467241058, 11.44779295918254824 ) ) ;
#90800=CARTESIAN_POINT ( 'NONE',  ( 13.37577147909557773, 18.27418014603220442, -1.500000000000002220 ) ) ;
#90801=B_SPLINE_CURVE_WITH_KNOTS ( 'NONE', 3,
 ( #6543, #77535, #47115, #91762, #46613, #78028 ),
 .UNSPECIFIED., .F., .F.,
 ( 4, 2, 4 ),
 ( 1.570755371634415583E-05, 0.001396183895866091439, 0.002776660238015838614 ),
 .UNSPECIFIED. ) ;
#90802=VERTEX_POINT ( 'NONE', #90480 ) ;
#90803=LINE ( 'NONE', #13659, #51446 ) ;
#90804=CARTESIAN_POINT ( 'NONE',  ( -61.59189125704995860, -29.50249900881161835, 7.371157290072014590 ) ) ;
#90805=CARTESIAN_POINT ( 'NONE',  ( 6.388261542594571019, -18.74682169789839392, 11.49999999999999645 ) ) ;
#90808=VERTEX_POINT ( 'NONE', #60549 ) ;
#90812=CARTESIAN_POINT ( 'NONE',  ( 14.26105141482337935, -16.23293960606763520, 11.49999999999998934 ) ) ;
#90814=CARTESIAN_POINT ( 'NONE',  ( 19.05472526407214673, 3.605321472892077050, -1.500000000000002220 ) ) ;
#90817=CARTESIAN_POINT ( 'NONE',  ( 18.46520180437041603, 7.126043738416648843, 11.49999999999998934 ) ) ;
#90818=ORIENTED_EDGE ( 'NONE', *, *, #10590, .F. ) ;
#90819=CARTESIAN_POINT ( 'NONE',  ( 12.22771034161782566, -16.27230226814707947, 11.49999999999999645 ) ) ;
#90823=ORIENTED_EDGE ( 'NONE', *, *, #21678, .F. ) ;
#90824=CARTESIAN_POINT ( 'NONE',  ( -30.59167141582165783, -24.92410949913933393, 1.600845668900849894 ) ) ;
#90825=CARTESIAN_POINT ( 'NONE',  ( -106.6228709571500559, -23.47596703998600631, 11.44779298504227860 ) ) ;
#90826=CARTESIAN_POINT ( 'NONE',  ( -105.6228709571500417, -29.50249982740957577, 7.747779886224967605 ) ) ;
#90827=CARTESIAN_POINT ( 'NONE',  ( -82.62287095715005592, -23.48786465467241413, 11.44779295918254647 ) ) ;
#90829=CARTESIAN_POINT ( 'NONE',  ( 1.781536345648733199, 20.00535218256611358, -1.500000000000002220 ) ) ;
#90831=VERTEX_POINT ( 'NONE', #4751 ) ;
#90834=CARTESIAN_POINT ( 'NONE',  ( -16.48365427610503886, -15.78576583860491489, 11.49999999999999645 ) ) ;
#90835=CARTESIAN_POINT ( 'NONE',  ( -30.47287095715008576, -24.97456920234173339, 2.208563660530530992 ) ) ;
#90836=FACE_OUTER_BOUND ( 'NONE', #12287, .T. ) ;
#90838=AXIS2_PLACEMENT_3D ( 'NONE', #520, #33468, #40089 ) ;
#90839=CARTESIAN_POINT ( 'NONE',  ( -123.5228709571500616, -29.50250243563736774, 8.947779886222134493 ) ) ;
#90840=EDGE_CURVE ( 'NONE', #41495, #58299, #50451, .T. ) ;
#90841=AXIS2_PLACEMENT_3D ( 'NONE', #81572, #19158, #27778 ) ;
#90844=CARTESIAN_POINT ( 'NONE',  ( -51.53941112929729940, -25.30419751004783890, 5.186272124421679841 ) ) ;
#90846=CARTESIAN_POINT ( 'NONE',  ( -13.67433444753018534, -15.09191755960682890, -1.500000000000002220 ) ) ;
#90848=CARTESIAN_POINT ( 'NONE',  ( 22.25235761598246143, -5.642936543268669780, -1.500000000000002220 ) ) ;
#90850=ORIENTED_EDGE ( 'NONE', *, *, #87451, .F. ) ;
#90851=CARTESIAN_POINT ( 'NONE',  ( -101.6228709571500701, -23.47596703998600631, 11.44779298504227683 ) ) ;
#90852=CARTESIAN_POINT ( 'NONE',  ( -94.55620429048339304, -23.48783264082478084, -1.443836473390064157 ) ) ;
#90853=CARTESIAN_POINT ( 'NONE',  ( -38.52287095715006870, -24.66019654487199730, 8.947790411086121054 ) ) ;
#90854=CARTESIAN_POINT ( 'NONE',  ( 16.87399902462237478, -12.92443306546820736, 11.49999999999999645 ) ) ;
#90856=ORIENTED_EDGE ( 'NONE', *, *, #27249, .T. ) ;
#90857=CARTESIAN_POINT ( 'NONE',  ( -7.471142097702432316, -20.87072022463130239, -1.500000000000002220 ) ) ;
#90858=CARTESIAN_POINT ( 'NONE',  ( -16.38011734009650411, 12.53836025512309149, -1.500000000000002220 ) ) ;
#90861=DIRECTION ( 'NONE',  ( 1.000000000000000000, 3.773278334444166432E-23, 8.201307841325785021E-29 ) ) ;
#90862=B_SPLINE_CURVE_WITH_KNOTS ( 'NONE', 3,
 ( #15282, #60490, #46245, #99511 ),
 .UNSPECIFIED., .F., .F.,
 ( 4, 4 ),
 ( 0.000000000000000000, 9.999999999998897304E-05 ),
 .UNSPECIFIED. ) ;
#90863=CARTESIAN_POINT ( 'NONE',  ( -36.52287095715006870, -24.64898659630367916, 1.056161002820819261 ) ) ;
#90864=VERTEX_POINT ( 'NONE', #97590 ) ;
#90865=ORIENTED_EDGE ( 'NONE', *, *, #60326, .F. ) ;
#90866=CARTESIAN_POINT ( 'NONE',  ( -76.52287095715007581, -29.50248528299804818, 1.056150453629038477 ) ) ;
#90867=B_SPLINE_CURVE_WITH_KNOTS ( 'NONE', 3,
 ( #36849, #50574, #66818, #65820 ),
 .UNSPECIFIED., .F., .F.,
 ( 4, 4 ),
 ( 0.000000000000000000, 9.999999999998900014E-05 ),
 .UNSPECIFIED. ) ;
#90868=CARTESIAN_POINT ( 'NONE',  ( -41.57627760764538749, -24.66019654487199375, 8.947790411086122830 ) ) ;
#90869=CARTESIAN_POINT ( 'NONE',  ( -94.62287095715005592, -24.64965695001469115, 8.947790433994180503 ) ) ;
#90870=CARTESIAN_POINT ( 'NONE',  ( -18.04518632387085830, 10.29925911722504317, -1.500000000000002220 ) ) ;
#90871=CARTESIAN_POINT ( 'NONE',  ( -8.334044162642690878, 20.12857247364870616, 11.49999999999999645 ) ) ;
#90872=CARTESIAN_POINT ( 'NONE',  ( -39.44865907921395376, -25.27406546170053048, 4.125344378457973527 ) ) ;
#90873=CARTESIAN_POINT ( 'NONE',  ( -122.2228709571500787, -23.47593901973090169, -1.443836447538996426 ) ) ;
#90875=CARTESIAN_POINT ( 'NONE',  ( -21.57557905285345612, -6.117077608415351087, 11.49999999999998934 ) ) ;
#90876=CARTESIAN_POINT ( 'NONE',  ( -51.29599548036032530, -25.31296608742942666, 4.016965581434211785 ) ) ;
#90877=EDGE_CURVE ( 'NONE', #40078, #55078, #67349, .T. ) ;
#90878=ORIENTED_EDGE ( 'NONE', *, *, #33047, .F. ) ;
#90879=CARTESIAN_POINT ( 'NONE',  ( -98.52287095715006160, -24.64965694238575011, 8.947790433994194714 ) ) ;
#90881=ORIENTED_EDGE ( 'NONE', *, *, #62270, .F. ) ;
#90884=CARTESIAN_POINT ( 'NONE',  ( -99.47252348226193419, -25.29900225115328283, 5.640920301989122976 ) ) ;
#90885=VERTEX_POINT ( 'NONE', #82365 ) ;
#90886=CARTESIAN_POINT ( 'NONE',  ( 21.14028111218437900, -2.610574537768086234, -1.500000000000002220 ) ) ;
#90887=ORIENTED_EDGE ( 'NONE', *, *, #68543, .F. ) ;
#90889=CARTESIAN_POINT ( 'NONE',  ( -11.20027426441765961, 17.80179601997297212, -1.500000000000002220 ) ) ;
#90891=CARTESIAN_POINT ( 'NONE',  ( 22.03932947713327906, 5.445304565557160359, -1.500000000000002220 ) ) ;
#90893=CARTESIAN_POINT ( 'NONE',  ( -113.5228709571500900, -23.72773821059536914, 11.05748984161097326 ) ) ;
#90894=B_SPLINE_CURVE_WITH_KNOTS ( 'NONE', 3,
 ( #15954, #78350, #1748, #8851 ),
 .UNSPECIFIED., .F., .F.,
 ( 4, 4 ),
 ( 1.866604411097509178E-09, 0.0003958024117146408984 ),
 .UNSPECIFIED. ) ;
#90896=CARTESIAN_POINT ( 'NONE',  ( -16.24880213243413607, 14.73142910551002238, -1.500000000000002220 ) ) ;
#90897=CARTESIAN_POINT ( 'NONE',  ( -87.59864562871899807, -23.73766607897671221, -1.055555164236430032 ) ) ;
#90899=CARTESIAN_POINT ( 'NONE',  ( -40.21512553332997442, -25.29405891411934348, 5.531795786000103021 ) ) ;
#90900=ADVANCED_FACE ( 'NONE', ( #74259 ), #68147, .F. ) ;
#90902=CARTESIAN_POINT ( 'NONE',  ( -84.50667423978107706, -24.35071581493543391, 9.817618358456027039 ) ) ;
#90904=EDGE_CURVE ( 'NONE', #13904, #89924, #42826, .T. ) ;
#90905=CARTESIAN_POINT ( 'NONE',  ( -126.6228709571500843, -23.47596703998600631, 11.44779298504227860 ) ) ;
#90907=DIRECTION ( 'NONE',  ( 0.000000000000000000, -2.173523156925980399E-06, 0.9999999999976378895 ) ) ;
#90908=CARTESIAN_POINT ( 'NONE',  ( 13.65650298889772962, 16.33668418983593185, -1.500000000000002220 ) ) ;
#90909=DIRECTION ( 'NONE',  ( -3.773278334453079030E-23, 0.9999999999976377785, 2.173523156925979128E-06 ) ) ;
#90910=EDGE_CURVE ( 'NONE', #25882, #49692, #85471, .T. ) ;
#90911=CARTESIAN_POINT ( 'NONE',  ( -81.48149462243459595, -29.50249666744127808, 6.293933732382250845 ) ) ;
#90912=CARTESIAN_POINT ( 'NONE',  ( -85.62652016793876442, -24.83618233451450408, 1.606449574219535270 ) ) ;
#90914=CARTESIAN_POINT ( 'NONE',  ( -32.62287095715004881, -23.47593901973091235, -1.443836447539013301 ) ) ;
#90915=ORIENTED_EDGE ( 'NONE', *, *, #61215, .F. ) ;
#90916=CARTESIAN_POINT ( 'NONE',  ( -99.22308953234012563, -25.14696225287006826, 7.022768084356811435 ) ) ;
#90917=CARTESIAN_POINT ( 'NONE',  ( 13.10555085358618221, -14.64361678476065087, 11.49999999999999645 ) ) ;
#90918=CARTESIAN_POINT ( 'NONE',  ( -75.58953762381672448, -24.99156044556202616, 7.747789690856173195 ) ) ;
#90920=EDGE_CURVE ( 'NONE', #24964, #28708, #40740, .T. ) ;
#90921=EDGE_LOOP ( 'NONE', ( #64297, #88390, #21848, #91602 ) ) ;
#90924=CARTESIAN_POINT ( 'NONE',  ( -25.53324729430006101, -24.92678253223225582, 5.128894466507167849 ) ) ;
#90926=CARTESIAN_POINT ( 'NONE',  ( 6.578723047037327909, -18.57437435983987584, -1.500000000000002220 ) ) ;
#90927=ORIENTED_EDGE ( 'NONE', *, *, #3081, .F. ) ;
#90929=CARTESIAN_POINT ( 'NONE',  ( -70.62287095715002749, -23.85196035786900381, -0.8779234886474986954 ) ) ;
#90931=ORIENTED_EDGE ( 'NONE', *, *, #55317, .F. ) ;
#90934=CARTESIAN_POINT ( 'NONE',  ( -81.88534077628074215, -25.23679622552714363, 6.293943003980942308 ) ) ;
#90935=CARTESIAN_POINT ( 'NONE',  ( -118.6267481313898173, -23.96119346886881374, -0.6495511937832023630 ) ) ;
#90936=CARTESIAN_POINT ( 'NONE',  ( -121.5895376238167245, -24.65952944569305316, 1.056160979905702790 ) ) ;
#90937=CARTESIAN_POINT ( 'NONE',  ( -124.6228709571500559, -23.47593901973091235, -1.443836447538997536 ) ) ;
#90938=CARTESIAN_POINT ( 'NONE',  ( -120.5895376238167103, -23.47593901973091235, -1.443836447538997536 ) ) ;
#90939=CARTESIAN_POINT ( 'NONE',  ( 1.534201407001029027, 19.92515851932037663, -1.500000000000002220 ) ) ;
#90941=CARTESIAN_POINT ( 'NONE',  ( -95.58953762381671027, -25.00182538069145366, 7.747789668545099317 ) ) ;
#90942=CARTESIAN_POINT ( 'NONE',  ( -0.03668282068714227157, -22.57511205935180598, 1.639801994305458699 ) ) ;
#90948=FACE_OUTER_BOUND ( 'NONE', #44443, .T. ) ;
#90949=CARTESIAN_POINT ( 'NONE',  ( -28.52287095715005805, -24.48836230353387222, 1.056161703005638719 ) ) ;
#90950=CARTESIAN_POINT ( 'NONE',  ( -107.5228709571501042, -24.66019654487199730, 8.947790411086115725 ) ) ;
#90954=CARTESIAN_POINT ( 'NONE',  ( -45.62287095715004881, -25.00182538069145011, 7.747789668545099317 ) ) ;
#90955=VERTEX_POINT ( 'NONE', #58545 ) ;
#90956=CARTESIAN_POINT ( 'NONE',  ( -100.6228709571500559, -29.50248528299804818, 1.056150453629042030 ) ) ;
#90958=VERTEX_POINT ( 'NONE', #19963 ) ;
#90959=CARTESIAN_POINT ( 'NONE',  ( -2.356373108420451334, 20.14613781377289214, -1.500000000000002220 ) ) ;
#90961=CARTESIAN_POINT ( 'NONE',  ( -49.62287095715003460, -24.51283580621364067, 0.6167428607019802556 ) ) ;
#90962=FACE_OUTER_BOUND ( 'NONE', #40815, .T. ) ;
#90963=VERTEX_POINT ( 'NONE', #81871 ) ;
#90964=CARTESIAN_POINT ( 'NONE',  ( -77.52287095715004739, -23.95044443724992078, 10.65354141964649415 ) ) ;
#90965=CARTESIAN_POINT ( 'NONE',  ( -105.6228709571500275, -25.00158670708909625, 2.256160236439166411 ) ) ;
#90967=CARTESIAN_POINT ( 'NONE',  ( 17.53424486177994623, -9.724335930198575895, -1.500000000000002220 ) ) ;
#90968=CARTESIAN_POINT ( 'NONE',  ( 13.68530018921192060, -16.06810839794082924, 11.49999999999999645 ) ) ;
#90970=CARTESIAN_POINT ( 'NONE',  ( -28.70172027432288431, -24.98211893518114124, 7.134191928894627388 ) ) ;
#90971=CARTESIAN_POINT ( 'NONE',  ( -70.54635493862706141, -24.40133493613049964, 9.663955038902802386 ) ) ;
#90972=CARTESIAN_POINT ( 'NONE',  ( 15.76968270297436625, 15.47746201419723100, -1.500000000000002220 ) ) ;
#90974=CARTESIAN_POINT ( 'NONE',  ( -6.383830130275963910, 19.51498944528526991, 11.49999999999998934 ) ) ;
#90975=CARTESIAN_POINT ( 'NONE',  ( -50.52287095715006160, -29.50249982740957577, 7.747779886224967605 ) ) ;
#90977=CARTESIAN_POINT ( 'NONE',  ( -114.5228709571500190, -24.66019654487200441, 8.947790411086110396 ) ) ;
#90982=ORIENTED_EDGE ( 'NONE', *, *, #45717, .T. ) ;
#90983=CARTESIAN_POINT ( 'NONE',  ( -114.5228709571500616, -29.50247984919015209, -1.443849546365048253 ) ) ;
#90986=CARTESIAN_POINT ( 'NONE',  ( 18.07347782881280907, 9.871946371954690491, -1.500000000000002220 ) ) ;
#90987=CARTESIAN_POINT ( 'NONE',  ( 17.62533924669398999, -12.40915598911231577, 11.49999999999999645 ) ) ;
#90988=ORIENTED_EDGE ( 'NONE', *, *, #88043, .F. ) ;
#90989=CARTESIAN_POINT ( 'NONE',  ( -110.5228709571500616, -29.50250243563736774, 8.947779886222136270 ) ) ;
#90991=CARTESIAN_POINT ( 'NONE',  ( -2.124831620219566730, 22.23837930986240607, -1.500000000000002220 ) ) ;
#90992=CARTESIAN_POINT ( 'NONE',  ( -80.05243144761681151, -25.27875073300474185, 7.021016647303503611 ) ) ;
#90993=CARTESIAN_POINT ( 'NONE',  ( -84.55098283564281303, -24.15543982623907482, -0.2315651400026630391 ) ) ;
#90995=FACE_OUTER_BOUND ( 'NONE', #66182, .T. ) ;
#90996=CARTESIAN_POINT ( 'NONE',  ( -35.52137790958372676, -24.92592662359560407, 8.075495903017991139 ) ) ;
#90997=CARTESIAN_POINT ( 'NONE',  ( -5.628781154649386664, 20.11113626451368219, -1.500000000000002220 ) ) ;
#90999=CARTESIAN_POINT ( 'NONE',  ( -86.50456855957719426, -24.51314013834314665, 0.6176544820404149538 ) ) ;
#91001=VERTEX_POINT ( 'NONE', #43322 ) ;
#91002=AXIS2_PLACEMENT_3D ( 'NONE', #85521, #38352, #93626 ) ;
#91003=DIRECTION ( 'NONE',  ( 0.000000000000000000, 0.9999999999976377785, 2.173523156925979128E-06 ) ) ;
#91004=CARTESIAN_POINT ( 'NONE',  ( -19.14942259116913092, -8.910193081567555851, -1.500000000000002220 ) ) ;
#91008=CARTESIAN_POINT ( 'NONE',  ( 20.45693200876408469, 7.529271608661172621, 11.49999999999998934 ) ) ;
#91009=DIRECTION ( 'NONE',  ( -3.773278334453079618E-23, 0.9999999999976377785, 2.173523156925979975E-06 ) ) ;
#91012=CARTESIAN_POINT ( 'NONE',  ( 2.995010171738120786, 21.53247193037183038, -1.500000000000002220 ) ) ;
#91013=CARTESIAN_POINT ( 'NONE',  ( -71.56719770743626441, -25.24674200897194254, 5.535760866200059027 ) ) ;
#91014=EDGE_CURVE ( 'NONE', #77171, #69183, #90338, .T. ) ;
#91015=CARTESIAN_POINT ( 'NONE',  ( 3.885606641962014329, -21.97303888676646721, 11.49999999999999645 ) ) ;
#91016=ORIENTED_EDGE ( 'NONE', *, *, #34618, .F. ) ;
#91019=LINE ( 'NONE', #13387, #78024 ) ;
#91020=ORIENTED_EDGE ( 'NONE', *, *, #34440, .T. ) ;
#91024=B_SPLINE_CURVE_WITH_KNOTS ( 'NONE', 3,
 ( #10132, #94366, #24853, #55827 ),
 .UNSPECIFIED., .F., .F.,
 ( 4, 4 ),
 ( 2.775557561562891351E-17, 0.0001000000000000167286 ),
 .UNSPECIFIED. ) ;
#91027=CARTESIAN_POINT ( 'NONE',  ( -49.74369414166532266, -25.30543060587212167, 4.940877950953177944 ) ) ;
#91030=CARTESIAN_POINT ( 'NONE',  ( -43.62287095715005592, -23.72773821059535848, 11.05748984161097503 ) ) ;
#91031=CARTESIAN_POINT ( 'NONE',  ( -5.798782886354239885, 18.49141925852020663, -1.500000000000002220 ) ) ;
#91032=CARTESIAN_POINT ( 'NONE',  ( -46.52287095715006160, -23.47596703998600631, 11.44779298504229104 ) ) ;
#91034=CARTESIAN_POINT ( 'NONE',  ( 5.650214204171827070, -18.61605495904187535, 11.49999999999999645 ) ) ;
#91040=CARTESIAN_POINT ( 'NONE',  ( -102.6228709571500843, -23.73907113216990794, -1.053371485793225482 ) ) ;
#91042=B_SPLINE_CURVE_WITH_KNOTS ( 'NONE', 3,
 ( #40867, #3820, #17528, #88548, #18525, #27147, #19024, #2320 ),
 .UNSPECIFIED., .F., .F.,
 ( 4, 2, 2, 4 ),
 ( 6.384118678612070021E-06, 0.002007151183507257120, 0.003007534715921578172, 0.004007918248335898791 ),
 .UNSPECIFIED. ) ;
#91043=AXIS2_PLACEMENT_3D ( 'NONE', #20292, #51768, #98920 ) ;
#91044=CARTESIAN_POINT ( 'NONE',  ( 16.84789977498956404, 10.09486508543780481, 11.49999999999998934 ) ) ;
#91045=CARTESIAN_POINT ( 'NONE',  ( -81.62287095715005592, -29.50250243563736774, 8.947779886222141599 ) ) ;
#91047=ORIENTED_EDGE ( 'NONE', *, *, #54772, .F. ) ;
#91048=CARTESIAN_POINT ( 'NONE',  ( 18.51311748589099082, 11.02308708543723270, 11.49999999999998934 ) ) ;
#91051=LINE ( 'NONE', #11934, #86490 ) ;
#91052=CARTESIAN_POINT ( 'NONE',  ( -100.3381132846150052, -25.27473222076016768, 3.296131264066584077 ) ) ;
#91053=CARTESIAN_POINT ( 'NONE',  ( 22.92345266703080142, -2.467471440992916154, -1.500000000000002220 ) ) ;
#91056=CARTESIAN_POINT ( 'NONE',  ( -49.53129519467806574, -24.65952944569304606, 1.056160979905696129 ) ) ;
#91057=CARTESIAN_POINT ( 'NONE',  ( 7.141438900065890216, -18.84860497471923679, 11.49999999999999645 ) ) ;
#91058=CARTESIAN_POINT ( 'NONE',  ( -45.62287095715004881, -24.91570333823099759, 8.075032458375549282 ) ) ;
#91061=DIRECTION ( 'NONE',  ( 0.000000000000000000, 2.173523156925980399E-06, -0.9999999999976378895 ) ) ;
#91062=CARTESIAN_POINT ( 'NONE',  ( -110.8177083405623478, -25.29779178145291496, 3.398758112327336267 ) ) ;
#91063=EDGE_CURVE ( 'NONE', #3935, #87407, #27454, .T. ) ;
#91064=CARTESIAN_POINT ( 'NONE',  ( 19.48829924427396421, 3.997931079995220127, -1.500000000000002220 ) ) ;
#91065=CARTESIAN_POINT ( 'NONE',  ( -113.5177925269431256, -24.15543982623907482, -0.2315651400026574047 ) ) ;
#91066=CARTESIAN_POINT ( 'NONE',  ( 9.261118129494249729, -17.44851725036260248, -1.500000000000002220 ) ) ;
#91068=ADVANCED_FACE ( 'NONE', ( #62034 ), #100406, .T. ) ;
#91069=CARTESIAN_POINT ( 'NONE',  ( -38.62287095715005592, -23.48786465467240703, 11.44779295918255180 ) ) ;
#91071=CARTESIAN_POINT ( 'NONE',  ( -20.66316395829706209, -0.6310838753663271516, 11.49999999999999645 ) ) ;
#91072=CARTESIAN_POINT ( 'NONE',  ( -111.6228709571500559, -24.64965695001468404, 8.947790433994176951 ) ) ;
#91075=CARTESIAN_POINT ( 'NONE',  ( 4.020035926878589905, 22.33396232419688587, 11.49999999999999645 ) ) ;
#91076=EDGE_CURVE ( 'NONE', #17028, #86907, #80641, .T. ) ;
#91077=ORIENTED_EDGE ( 'NONE', *, *, #65661, .T. ) ;
#91078=B_SPLINE_SURFACE_WITH_KNOTS ( 'NONE', 3, 3, ( 
 ( #21567, #68267, #49311, #26466 ),
 ( #25452, #87348, #95463, #17848 ),
 ( #73140, #25954, #48809, #10735 ),
 ( #11231, #18345, #94963, #33572 ),
 ( #64550, #88359, #56426, #42208 ),
 ( #80748, #80242, #79734, #41189 ),
 ( #56926, #87857, #41700, #72643 ) ),
 .UNSPECIFIED., .F., .F., .F.,
 ( 4, 3, 4 ),
 ( 4, 4 ),
 ( 0.7945040050992232539, 0.8970133687736492334, 0.9995227324480751019 ),
 ( 0.02950149398476096044, 0.03052783838704493588 ),
 .UNSPECIFIED. ) ;
#91079=CARTESIAN_POINT ( 'NONE',  ( -60.62287095715004881, -23.48783264082478439, -1.443836473390068820 ) ) ;
#91081=CARTESIAN_POINT ( 'NONE',  ( -4.116507902937485142, 19.75820112358731251, -1.500000000000002220 ) ) ;
#91084=ORIENTED_EDGE ( 'NONE', *, *, #43371, .F. ) ;
#91087=CARTESIAN_POINT ( 'NONE',  ( 11.15996004898972771, 19.99216496293481882, -1.500000000000002220 ) ) ;
#91089=CARTESIAN_POINT ( 'NONE',  ( -8.750087785235610482, 19.73178376063210138, -1.500000000000002220 ) ) ;
#91090=CARTESIAN_POINT ( 'NONE',  ( -123.5900408317157400, -24.15543982623907482, -0.2315651400026560169 ) ) ;
#91091=DIRECTION ( 'NONE',  ( -3.773278334453079618E-23, 0.9999999999976377785, 2.173523156925978705E-06 ) ) ;
#91092=CARTESIAN_POINT ( 'NONE',  ( 19.01167203989450982, 12.12494712425435850, 11.49999999999999645 ) ) ;
#91093=ORIENTED_EDGE ( 'NONE', *, *, #93681, .F. ) ;
#91094=CARTESIAN_POINT ( 'NONE',  ( -86.92287095715005307, -23.47593901973090169, -1.443836447538996870 ) ) ;
#91096=CARTESIAN_POINT ( 'NONE',  ( 16.65356921002588919, 14.36988287374134821, 11.49999999999998934 ) ) ;
#91097=B_SPLINE_CURVE_WITH_KNOTS ( 'NONE', 3,
 ( #55474, #39732, #17402, #80302, #41246, #48362 ),
 .UNSPECIFIED., .F., .F.,
 ( 4, 2, 4 ),
 ( 1.570755371633915156E-05, 0.001396183895866087753, 0.002776660238015836446 ),
 .UNSPECIFIED. ) ;
#91100=CARTESIAN_POINT ( 'NONE',  ( -28.09930172958063466, -25.21724980323388010, 7.540557109994362683 ) ) ;
#91103=CARTESIAN_POINT ( 'NONE',  ( -90.62774790572264294, -24.73531770709095312, 8.716586749053512051 ) ) ;
#91105=CARTESIAN_POINT ( 'NONE',  ( -72.59671265881189584, -23.96169478059713143, 10.65365249895718414 ) ) ;
#91107=VERTEX_POINT ( 'NONE', #51231 ) ;
#91109=CARTESIAN_POINT ( 'NONE',  ( -49.31882137186372717, -25.28401378673735067, 5.880832581787514890 ) ) ;
#91110=PLANE ( 'NONE',  #3268 ) ;
#91111=CARTESIAN_POINT ( 'NONE',  ( -57.55356396053624479, -23.96119346886880663, -0.6495511937832122440 ) ) ;
#91112=CARTESIAN_POINT ( 'NONE',  ( -15.93830457579706739, -12.76012858937699335, -1.500000000000002220 ) ) ;
#91113=ORIENTED_EDGE ( 'NONE', *, *, #16259, .T. ) ;
#91116=CARTESIAN_POINT ( 'NONE',  ( -99.52287095715001897, -24.51387760970726504, 9.387446482453416507 ) ) ;
#91117=EDGE_CURVE ( 'NONE', #33243, #56669, #10553, .T. ) ;
#91118=VECTOR ( 'NONE', #60968, 1000.000000000000114 ) ;
#91120=DIRECTION ( 'NONE',  ( 0.000000000000000000, -2.173523156925979552E-06, 0.9999999999976378895 ) ) ;
#91123=CARTESIAN_POINT ( 'NONE',  ( -28.90723246652128609, -25.26247981585383684, 7.813648767477532786 ) ) ;
#91125=CARTESIAN_POINT ( 'NONE',  ( -2.100290975465340271, -20.70549805216813510, -1.500000000000002220 ) ) ;
#91126=ORIENTED_EDGE ( 'NONE', *, *, #5787, .F. ) ;
#91130=ORIENTED_EDGE ( 'NONE', *, *, #51205, .T. ) ;
#91131=VERTEX_POINT ( 'NONE', #2567 ) ;
#91132=CARTESIAN_POINT ( 'NONE',  ( -120.6228709571500417, -23.47593901973091235, -1.443836447538997536 ) ) ;
#91134=AXIS2_PLACEMENT_3D ( 'NONE', #20485, #97615, #65702 ) ;
#91135=CARTESIAN_POINT ( 'NONE',  ( -60.58953762381672448, -23.48786465467241058, 11.44779295918254824 ) ) ;
#91136=DIRECTION ( 'NONE',  ( -3.773278334453079030E-23, 0.9999999999976377785, 2.173523156925979128E-06 ) ) ;
#91137=ADVANCED_FACE ( 'NONE', ( #57865 ), #66348, .T. ) ;
#91138=CARTESIAN_POINT ( 'NONE',  ( 0.7503028313155074569, 22.12739137992853955, 11.49999999999999645 ) ) ;
#91140=CARTESIAN_POINT ( 'NONE',  ( -72.62287095715005592, -24.65952944569304606, 1.056160979905698794 ) ) ;
#91141=CARTESIAN_POINT ( 'NONE',  ( 21.95517018727266390, 5.574673621280945568, -1.500000000000002220 ) ) ;
#91142=CARTESIAN_POINT ( 'NONE',  ( -92.52287095715011844, -23.96127896942171276, -0.6493128930931688636 ) ) ;
#91143=ORIENTED_EDGE ( 'NONE', *, *, #547, .F. ) ;
#91147=AXIS2_PLACEMENT_3D ( 'NONE', #48760, #95417, #32013 ) ;
#91148=CARTESIAN_POINT ( 'NONE',  ( -18.22032804147677254, 8.545885342870345625, -1.500000000000002220 ) ) ;
#91153=CARTESIAN_POINT ( 'NONE',  ( -6.278373996654322831, -21.41630973362384083, -1.500000000000002220 ) ) ;
#91154=EDGE_CURVE ( 'NONE', #67264, #76612, #35887, .T. ) ;
#91155=ORIENTED_EDGE ( 'NONE', *, *, #11007, .T. ) ;
#91156=ORIENTED_EDGE ( 'NONE', *, *, #36061, .T. ) ;
#91158=DIRECTION ( 'NONE',  ( 0.000000000000000000, 0.9999999999976377785, 2.173523156925979128E-06 ) ) ;
#91159=FACE_OUTER_BOUND ( 'NONE', #41111, .T. ) ;
#91160=CARTESIAN_POINT ( 'NONE',  ( -96.62287095715005592, -24.66019654487199730, 8.947790411086124607 ) ) ;
#91161=ADVANCED_FACE ( 'NONE', ( #6049 ), #59853, .T. ) ;
#91162=CARTESIAN_POINT ( 'NONE',  ( -44.22287095715005023, -23.47596703998600276, 11.44779298504227860 ) ) ;
#91164=CARTESIAN_POINT ( 'NONE',  ( 14.28107258077893604, -13.35224110012613963, 11.49999999999998934 ) ) ;
#91165=AXIS2_PLACEMENT_3D ( 'NONE', #34664, #10318, #27554 ) ;
#91167=CARTESIAN_POINT ( 'NONE',  ( -14.42888051209446409, 15.91495273949476363, 11.49999999999998934 ) ) ;
#91168=CARTESIAN_POINT ( 'NONE',  ( -25.89225704477708589, -24.92774936967245125, 2.873802147424679987 ) ) ;
#91169=LINE ( 'NONE', #52613, #40588 ) ;
#91171=CARTESIAN_POINT ( 'NONE',  ( -13.85039312988123150, 18.09399583546626289, -1.500000000000002220 ) ) ;
#91172=CARTESIAN_POINT ( 'NONE',  ( -96.54970709809541063, -24.35071581493543391, 9.817618358456023486 ) ) ;
#91173=CARTESIAN_POINT ( 'NONE',  ( -91.62287095715004170, -29.50250786944525672, 11.44777988621623344 ) ) ;
#91174=CARTESIAN_POINT ( 'NONE',  ( 19.59856454566043382, -3.714209461170434157, 11.49999999999999645 ) ) ;
#91175=CARTESIAN_POINT ( 'NONE',  ( -59.62287095715004881, -29.50248528299804818, 1.056150453629034924 ) ) ;
#91178=ORIENTED_EDGE ( 'NONE', *, *, #24101, .F. ) ;
#91179=DIRECTION ( 'NONE',  ( 3.773278334444166432E-23, -1.000000000000000000, 0.000000000000000000 ) ) ;
#91181=CARTESIAN_POINT ( 'NONE',  ( -19.66401359581072583, -9.230316601043258018, 11.49999999999998934 ) ) ;
#91183=CARTESIAN_POINT ( 'NONE',  ( 14.99095386781537975, 12.61000069877385421, -1.500000000000002220 ) ) ;
#91184=CARTESIAN_POINT ( 'NONE',  ( -80.62287095715005592, -24.99156045073393173, 7.747789690856161648 ) ) ;
#91185=AXIS2_PLACEMENT_3D ( 'NONE', #45385, #61613, #75805 ) ;
#91190=CARTESIAN_POINT ( 'NONE',  ( -54.62287095715005592, -29.50248528299804818, 1.056150453629033370 ) ) ;
#91191=CARTESIAN_POINT ( 'NONE',  ( 20.32696876622996029, 2.630761579057304900, 11.49999999999999645 ) ) ;
#91192=CARTESIAN_POINT ( 'NONE',  ( -39.06125964696975217, -25.30336593734606510, 4.454089851809797551 ) ) ;
#91194=CARTESIAN_POINT ( 'NONE',  ( -93.62287095715004170, -23.48783264082478794, -1.443836473390063713 ) ) ;
#91196=VERTEX_POINT ( 'NONE', #45128 ) ;
#91198=DIRECTION ( 'NONE',  ( 1.000000000000000000, 3.773278334444167608E-23, 8.201307833595939069E-29 ) ) ;
#91201=DIRECTION ( 'NONE',  ( -3.773278334453080206E-23, 0.9999999999976377785, 2.173523156925979975E-06 ) ) ;
#91204=CARTESIAN_POINT ( 'NONE',  ( 21.75825945658488436, -7.631246777643061030, 11.49999999999999645 ) ) ;
#91205=CARTESIAN_POINT ( 'NONE',  ( -9.359374538088376383, 20.77767741201286711, -1.500000000000002220 ) ) ;
#91207=B_SPLINE_SURFACE_WITH_KNOTS ( 'NONE', 3, 3, ( 
 ( #96594, #42829, #79368, #33199 ),
 ( #65185, #33707, #57559, #50432 ),
 ( #9862, #34213, #73760, #27597 ),
 ( #17979, #96109, #89487, #25587 ),
 ( #19966, #48940, #79868, #40812 ),
 ( #2768, #88495, #18971, #66180 ),
 ( #42339, #49949, #64181, #95102 ) ),
 .UNSPECIFIED., .F., .F., .F.,
 ( 4, 3, 4 ),
 ( 4, 4 ),
 ( 0.0004766839783816845776, 0.1029713700210893035, 0.2054660560637969202 ),
 ( 0.5796414481296850996, 0.5809216181848338989 ),
 .UNSPECIFIED. ) ;
#91208=CARTESIAN_POINT ( 'NONE',  ( -105.6228709571500559, -23.47593901973091235, -1.443836447538999312 ) ) ;
#91210=LINE ( 'NONE', #52160, #25246 ) ;
#91212=CARTESIAN_POINT ( 'NONE',  ( 11.25260618158950621, 18.78031238747207610, 11.49999999999998934 ) ) ;
#91213=DIRECTION ( 'NONE',  ( 0.000000000000000000, -0.9999999999976377785, -2.173523156925979975E-06 ) ) ;
#91215=CARTESIAN_POINT ( 'NONE',  ( -50.62287095715007013, -24.52232992886362695, 0.6492154411906128075 ) ) ;
#91216=CARTESIAN_POINT ( 'NONE',  ( -40.48073109628643351, -25.31533619740083196, 5.080591194951591838 ) ) ;
#91217=CARTESIAN_POINT ( 'NONE',  ( -78.62361334277453295, -24.65952944569304606, 1.056160979905704789 ) ) ;
#91218=CARTESIAN_POINT ( 'NONE',  ( -112.6228709571500559, -23.47593901973091235, -1.443836447538999312 ) ) ;
#91220=ORIENTED_EDGE ( 'NONE', *, *, #23758, .F. ) ;
#91221=CARTESIAN_POINT ( 'NONE',  ( -4.302178748239556150, -20.00421716419250373, 11.49999999999998934 ) ) ;
#91224=EDGE_LOOP ( 'NONE', ( #56468, #44682, #12139, #10268 ) ) ;
#91226=CARTESIAN_POINT ( 'NONE',  ( -20.34888222059871410, 10.79260868881566715, -1.500000000000002220 ) ) ;
#91227=CARTESIAN_POINT ( 'NONE',  ( -35.52287095715006870, -24.52232992886611740, 0.6492154411976478467 ) ) ;
#91228=CARTESIAN_POINT ( 'NONE',  ( -13.42616926349082895, -15.17935092467416069, -1.500000000000002220 ) ) ;
#91230=ORIENTED_EDGE ( 'NONE', *, *, #90904, .T. ) ;
#91231=EDGE_CURVE ( 'NONE', #100041, #82077, #65040, .T. ) ;
#91232=CARTESIAN_POINT ( 'NONE',  ( -48.52287095715006160, -23.47596703998600631, 11.44779298504229104 ) ) ;
#91233=EDGE_CURVE ( 'NONE', #80383, #14468, #21757, .T. ) ;
#91237=CARTESIAN_POINT ( 'NONE',  ( -70.56769351002753865, -23.48783264082477018, -1.443836473390095021 ) ) ;
#91238=CARTESIAN_POINT ( 'NONE',  ( 20.52986552169224410, -6.224258026782483633, 11.49999999999999645 ) ) ;
#91239=ORIENTED_EDGE ( 'NONE', *, *, #52797, .F. ) ;
#91240=DIRECTION ( 'NONE',  ( 1.000000000000000000, 3.773278334444167608E-23, 8.201307833595939069E-29 ) ) ;
#91245=CARTESIAN_POINT ( 'NONE',  ( -19.59449498831206782, -6.737714454370689054, -1.500000000000002220 ) ) ;
#91247=ORIENTED_EDGE ( 'NONE', *, *, #91905, .T. ) ;
#91248=CARTESIAN_POINT ( 'NONE',  ( -28.51175871785264349, -23.57346878409127200, -1.055554491438110309 ) ) ;
#91251=ORIENTED_EDGE ( 'NONE', *, *, #80510, .T. ) ;
#91252=CARTESIAN_POINT ( 'NONE',  ( 2.184583272949580213, -20.89682302726931340, -1.500000000000002220 ) ) ;
#91254=CARTESIAN_POINT ( 'NONE',  ( 11.39931579351042679, 18.75040340349860557, 11.49999999999999645 ) ) ;
#91256=CARTESIAN_POINT ( 'NONE',  ( 18.83488669200175281, -12.41447709603701632, -1.500000000000002220 ) ) ;
#91257=CARTESIAN_POINT ( 'NONE',  ( -12.80012119340476140, -16.60591428456014640, 11.49999999999998934 ) ) ;
#91258=CARTESIAN_POINT ( 'NONE',  ( -89.62287095715004170, -24.64898659630529210, 1.056161002820827921 ) ) ;
#91261=CARTESIAN_POINT ( 'NONE',  ( -53.55620429048339304, -23.48786465467240347, 11.44779295918255002 ) ) ;
#91262=ORIENTED_EDGE ( 'NONE', *, *, #71322, .F. ) ;
#91264=B_SPLINE_CURVE_WITH_KNOTS ( 'NONE', 3,
 ( #83661, #99868, #30375, #44612 ),
 .UNSPECIFIED., .F., .F.,
 ( 4, 4 ),
 ( 1.301246609561020917E-05, 0.002190852597862436284 ),
 .UNSPECIFIED. ) ;
#91269=EDGE_CURVE ( 'NONE', #14852, #47263, #21311, .T. ) ;
#91270=CARTESIAN_POINT ( 'NONE',  ( 15.57385778016992894, -14.83193121981731544, -1.500000000000002220 ) ) ;
#91273=ORIENTED_EDGE ( 'NONE', *, *, #75245, .T. ) ;
#91274=CARTESIAN_POINT ( 'NONE',  ( 11.07546443054301655, -17.96822238807187233, -1.500000000000002220 ) ) ;
#91275=CARTESIAN_POINT ( 'NONE',  ( -81.52287095715006160, -29.50247984919015209, -1.443849546365053582 ) ) ;
#91276=CARTESIAN_POINT ( 'NONE',  ( -64.49572739054461579, -24.51314013834315730, 0.6176544820404094027 ) ) ;
#91277=CARTESIAN_POINT ( 'NONE',  ( -49.62287095715005592, -23.48783264082478084, -1.443836473390070596 ) ) ;
#91279=PLANE ( 'NONE',  #43834 ) ;
#91280=CARTESIAN_POINT ( 'NONE',  ( -19.76278938440450617, -9.944092408650034187, -1.500000000000002220 ) ) ;
#91282=CARTESIAN_POINT ( 'NONE',  ( -81.54381818738237087, -24.51419770103159834, 9.386484678747182286 ) ) ;
#91283=ADVANCED_FACE ( 'NONE', ( #9047 ), #50937, .T. ) ;
#91288=EDGE_CURVE ( 'NONE', #12640, #25116, #57651, .T. ) ;
#91289=CARTESIAN_POINT ( 'NONE',  ( -97.52287095715009002, -23.72773821059536914, 11.05748984161097503 ) ) ;
#91290=CARTESIAN_POINT ( 'NONE',  ( 9.746180923669104601, -16.83516941858706417, -1.500000000000002220 ) ) ;
#91291=CARTESIAN_POINT ( 'NONE',  ( -18.12654925440673637, -11.31956730046968751, -1.500000000000002220 ) ) ;
#91292=CARTESIAN_POINT ( 'NONE',  ( -113.6228709571500559, -23.48786465467241769, 11.44779295918254114 ) ) ;
#91293=CARTESIAN_POINT ( 'NONE',  ( -81.52287095715006160, -23.48786465467241058, 11.44779295918254469 ) ) ;
#91294=CARTESIAN_POINT ( 'NONE',  ( -72.52287095715011844, -24.33927499327855770, 9.819080762295822495 ) ) ;
#91295=CARTESIAN_POINT ( 'NONE',  ( -36.62287095715005592, -24.66019654487199020, 8.947790411086138818 ) ) ;
#91296=CARTESIAN_POINT ( 'NONE',  ( -13.31036990564671818, -18.29084955798148471, -1.500000000000002220 ) ) ;
#91297=B_SPLINE_SURFACE_WITH_KNOTS ( 'NONE', 3, 3, ( 
 ( #45892, #92052, #21038, #29158 ),
 ( #60132, #6814, #37278, #5322 ),
 ( #68727, #61123, #52507, #59129 ),
 ( #68229, #99158, #52007, #82937 ) ),
 .UNSPECIFIED., .F., .F., .F.,
 ( 4, 4 ),
 ( 4, 4 ),
 ( 0.3744551372274605994, 0.4812677536984230064 ),
 ( 0.7926673770166410282, 0.8107671855866930288 ),
 .UNSPECIFIED. ) ;
#91298=ORIENTED_EDGE ( 'NONE', *, *, #50155, .F. ) ;
#91299=CARTESIAN_POINT ( 'NONE',  ( -80.96226385320382235, -29.50248939449842922, 2.947779886236309377 ) ) ;
#91300=CARTESIAN_POINT ( 'NONE',  ( -89.49044894935767047, -29.50248914370730091, 2.832395270851967073 ) ) ;
#91301=CARTESIAN_POINT ( 'NONE',  ( -16.86558833231006460, 10.32443627698238409, 11.49999999999999645 ) ) ;
#91302=CARTESIAN_POINT ( 'NONE',  ( -91.62287095715004170, -23.47593901973091235, -1.443836447539002865 ) ) ;
#91304=DIRECTION ( 'NONE',  ( -3.773278334453079030E-23, 0.9999999999976377785, 2.173523156925979128E-06 ) ) ;
#91307=CARTESIAN_POINT ( 'NONE',  ( 7.043455336710909620, -20.48365140995157674, 11.49999999999998934 ) ) ;
#91308=CARTESIAN_POINT ( 'NONE',  ( -49.47157371846719087, -25.10935202069072858, 3.177618851823707402 ) ) ;
#91309=CARTESIAN_POINT ( 'NONE',  ( 19.04819733361787470, -3.913502273677552878, -1.500000000000002220 ) ) ;
#91312=CARTESIAN_POINT ( 'NONE',  ( 18.78060722631472501, -6.265068672152646734, -1.500000000000002220 ) ) ;
#91315=CARTESIAN_POINT ( 'NONE',  ( -20.26613141553852060, -1.498020344548873561, 11.49999999999999645 ) ) ;
#91319=CARTESIAN_POINT ( 'NONE',  ( -102.6290224326610172, -24.15620529776628445, 10.23563542870660292 ) ) ;
#91320=CARTESIAN_POINT ( 'NONE',  ( -116.4728709594060092, -25.40676080801055647, 8.000950338065035083 ) ) ;
#91321=FACE_OUTER_BOUND ( 'NONE', #69278, .T. ) ;
#91323=CARTESIAN_POINT ( 'NONE',  ( -51.22478625508527728, -25.16632228261309123, 6.837805518550829298 ) ) ;
#91324=CARTESIAN_POINT ( 'NONE',  ( 2.879247915899910470, -19.84986158617241614, 11.49999999999998934 ) ) ;
#91327=CARTESIAN_POINT ( 'NONE',  ( -116.5228709571500616, -29.50247984919015209, -1.443849546365046699 ) ) ;
#91328=CARTESIAN_POINT ( 'NONE',  ( -18.62658236799572720, 13.20813282334384553, 11.49999999999999645 ) ) ;
#91329=CARTESIAN_POINT ( 'NONE',  ( -49.51279233427662518, -25.26258742029363447, 4.076580261917981396 ) ) ;
#91333=CARTESIAN_POINT ( 'NONE',  ( -88.88918693012689687, -29.50249691823240994, 6.409318347766594037 ) ) ;
#91338=CARTESIAN_POINT ( 'NONE',  ( -20.15914900662387055, -2.930279687489938389, -1.500000000000002220 ) ) ;
#91342=CARTESIAN_POINT ( 'NONE',  ( 16.23347398924790497, -16.23827457187686463, 11.49999999999998934 ) ) ;
#91343=CARTESIAN_POINT ( 'NONE',  ( -37.55620429048340725, -24.65952944569304250, 1.056160979905692132 ) ) ;
#91346=CARTESIAN_POINT ( 'NONE',  ( -108.5148028597040337, -24.35071581493544457, 9.817618358456016381 ) ) ;
#91349=CARTESIAN_POINT ( 'NONE',  ( -51.54139007992708343, -24.35071581493542681, 9.817618358456028815 ) ) ;
#91350=CARTESIAN_POINT ( 'NONE',  ( 18.67678363807796416, 10.12720680154768971, 11.49999999999999645 ) ) ;
#91353=CARTESIAN_POINT ( 'NONE',  ( 22.14152233036116257, 1.636640089565777334, 11.49999999999998934 ) ) ;
#91354=CARTESIAN_POINT ( 'NONE',  ( -19.87711886888390822, 5.503898473480427711, -1.500000000000002220 ) ) ;
#91356=ORIENTED_EDGE ( 'NONE', *, *, #40780, .T. ) ;
#91357=PLANE ( 'NONE',  #81966 ) ;
#91358=B_SPLINE_CURVE_WITH_KNOTS ( 'NONE', 3,
 ( #52259, #58384, #50765, #12180 ),
 .UNSPECIFIED., .F., .F.,
 ( 4, 4 ),
 ( 0.000000000000000000, 9.999999999998900014E-05 ),
 .UNSPECIFIED. ) ;
#91361=ORIENTED_EDGE ( 'NONE', *, *, #43474, .F. ) ;
#91363=CARTESIAN_POINT ( 'NONE',  ( -41.62371469989763284, -24.66019654487199375, 8.947790411086122830 ) ) ;
#91365=CARTESIAN_POINT ( 'NONE',  ( 15.94631523246878579, 13.42178585792578360, -1.500000000000002220 ) ) ;
#91366=CARTESIAN_POINT ( 'NONE',  ( 8.287826148123016878, -20.17477452812186201, 11.49999999999999645 ) ) ;
#91368=CARTESIAN_POINT ( 'NONE',  ( -40.62552394256396582, -25.27806136706950468, 5.067902527831130932 ) ) ;
#91369=CARTESIAN_POINT ( 'NONE',  ( -52.52287095715005449, -23.47593901973090524, -1.443836447538997092 ) ) ;
#91370=CARTESIAN_POINT ( 'NONE',  ( -20.53624283083718893, 9.024085183690161216, 11.49999999999998934 ) ) ;
#91371=CARTESIAN_POINT ( 'NONE',  ( -50.88361436997121245, -25.26334723850860442, 4.608108886914586755 ) ) ;
#91373=DIRECTION ( 'NONE',  ( 0.000000000000000000, 0.9999999999976377785, 2.173523156925979552E-06 ) ) ;
#91374=CARTESIAN_POINT ( 'NONE',  ( -51.40669398549582780, -25.17894756043024884, 3.249225598437226470 ) ) ;
#91376=ORIENTED_EDGE ( 'NONE', *, *, #3614, .F. ) ;
#91380=CARTESIAN_POINT ( 'NONE',  ( 2.936642053869352953, -21.15864249054145674, -1.500000000000002220 ) ) ;
#91381=VERTEX_POINT ( 'NONE', #38502 ) ;
#91383=CARTESIAN_POINT ( 'NONE',  ( -20.73700405699343463, 3.470425206167693233, 11.49999999999998934 ) ) ;
#91384=FACE_OUTER_BOUND ( 'NONE', #66828, .T. ) ;
#91385=CARTESIAN_POINT ( 'NONE',  ( -111.3776484685884469, -25.29712067403330877, 4.332404411321261861 ) ) ;
#91386=DIRECTION ( 'NONE',  ( -1.000000000000000000, -3.773278334444166432E-23, -8.201307841325785021E-29 ) ) ;
#91387=CARTESIAN_POINT ( 'NONE',  ( 21.74639208212181529, -2.611101805624240768, -1.500000000000002220 ) ) ;
#91388=CARTESIAN_POINT ( 'NONE',  ( -87.55130954339645655, -24.15543982623908192, -0.2315651400026449980 ) ) ;
#91389=ORIENTED_EDGE ( 'NONE', *, *, #87373, .T. ) ;
#91390=CARTESIAN_POINT ( 'NONE',  ( -122.5557265984356121, -23.96169478059714564, 10.65365249895717170 ) ) ;
#91391=EDGE_CURVE ( 'NONE', #94778, #96462, #18991, .T. ) ;
#91392=CARTESIAN_POINT ( 'NONE',  ( -84.54748922658383492, -24.35071581493543391, 9.817618358456027039 ) ) ;
#91393=CARTESIAN_POINT ( 'NONE',  ( -130.5728709571501156, -24.04668586515359863, 10.47594215909544069 ) ) ;
#91394=CARTESIAN_POINT ( 'NONE',  ( -0.05748996396964650701, -22.30574723846597607, 8.909134979017292011 ) ) ;
#91395=CARTESIAN_POINT ( 'NONE',  ( 14.87313431965483801, 15.23822737908125902, 11.49999999999998934 ) ) ;
#91396=CARTESIAN_POINT ( 'NONE',  ( -98.55007674334730439, -24.35071581493543391, 9.817618358456027039 ) ) ;
#91397=CARTESIAN_POINT ( 'NONE',  ( -54.58953762381672448, -23.47593901973091235, -1.443836447539009749 ) ) ;
#91399=CARTESIAN_POINT ( 'NONE',  ( -60.62287095715004881, -23.47596703998600631, 11.44779298504227505 ) ) ;
#91400=CARTESIAN_POINT ( 'NONE',  ( -33.66791791009761425, -23.48783264082477729, -1.443836473390078368 ) ) ;
#91401=CARTESIAN_POINT ( 'NONE',  ( 17.77913403553526805, 13.70458096452923691, -1.500000000000002220 ) ) ;
#91402=CARTESIAN_POINT ( 'NONE',  ( -60.52287095715006160, -25.00158670708908915, 2.256160236439166411 ) ) ;
#91403=EDGE_LOOP ( 'NONE', ( #98986, #88604, #8624, #84420 ) ) ;
#91405=CARTESIAN_POINT ( 'NONE',  ( -17.63651738508609412, 8.604534254076446231, 11.49999999999999645 ) ) ;
#91408=ORIENTED_EDGE ( 'NONE', *, *, #73141, .T. ) ;
#91409=FACE_OUTER_BOUND ( 'NONE', #96847, .T. ) ;
#91410=DIRECTION ( 'NONE',  ( -1.000000000000000000, -3.773278334444166432E-23, -8.201307841325785021E-29 ) ) ;
#91411=CARTESIAN_POINT ( 'NONE',  ( -89.90088307144425528, -25.32379766982192493, 4.367815445636562544 ) ) ;
#91412=B_SPLINE_CURVE_WITH_KNOTS ( 'NONE', 3,
 ( #11380, #18491, #66196, #73288, #59068, #27108 ),
 .UNSPECIFIED., .F., .F.,
 ( 4, 2, 4 ),
 ( 1.570755371634454886E-05, 0.001396183895866089488, 0.002776660238015834711 ),
 .UNSPECIFIED. ) ;
#91414=CARTESIAN_POINT ( 'NONE',  ( -19.65353550717971487, 1.628721094194526486, -1.500000000000002220 ) ) ;
#91416=FACE_OUTER_BOUND ( 'NONE', #3213, .T. ) ;
#91417=DIRECTION ( 'NONE',  ( 0.000000000000000000, -0.9999999999976377785, -2.173523156925979128E-06 ) ) ;
#91420=EDGE_LOOP ( 'NONE', ( #5509, #88930, #45183, #12751 ) ) ;
#91421=DIRECTION ( 'NONE',  ( 0.000000000000000000, -0.9999999999976377785, -2.173523156925979975E-06 ) ) ;
#91422=CARTESIAN_POINT ( 'NONE',  ( -84.62287095715005592, -23.48783264082479150, -1.443836473390065489 ) ) ;
#91423=CARTESIAN_POINT ( 'NONE',  ( -55.53423014570002181, -24.73486907724917572, 1.287355809206960355 ) ) ;
#91425=CARTESIAN_POINT ( 'NONE',  ( -121.6228709571500417, -24.65952944569305316, 1.056160979905705677 ) ) ;
#91427=CARTESIAN_POINT ( 'NONE',  ( -107.6297646753413346, -23.96119346886881374, -0.6495511937831857097 ) ) ;
#91428=CARTESIAN_POINT ( 'NONE',  ( -19.24466553037914807, -5.328869878250761971, -1.500000000000002220 ) ) ;
#91429=VECTOR ( 'NONE', #9872, 1000.000000000000114 ) ;
#91430=CARTESIAN_POINT ( 'NONE',  ( -125.6228709571500559, -23.48786465467241769, 11.44779295918253403 ) ) ;
#91431=CARTESIAN_POINT ( 'NONE',  ( -45.48069253931505784, -24.73531770709094957, 8.716586749053515604 ) ) ;
#91434=B_SPLINE_CURVE_WITH_KNOTS ( 'NONE', 3,
 ( #402, #55212, #70422, #63836 ),
 .UNSPECIFIED., .F., .F.,
 ( 4, 4 ),
 ( 0.9894921560719619480, 0.9904929031127274186 ),
 .UNSPECIFIED. ) ;
#91435=CARTESIAN_POINT ( 'NONE',  ( -129.6228709571500417, -23.47596703998600631, 11.44779298504227683 ) ) ;
#91436=CARTESIAN_POINT ( 'NONE',  ( -80.51502784577047578, -23.85049219812685806, 10.88485053497527311 ) ) ;
#91438=CARTESIAN_POINT ( 'NONE',  ( -39.62888266615128430, -24.51314013834315730, 0.6176544820404118452 ) ) ;
#91442=DIRECTION ( 'NONE',  ( -3.773278334453079618E-23, 0.9999999999976377785, 2.173523156925979975E-06 ) ) ;
#91443=EDGE_LOOP ( 'NONE', ( #13850, #30177, #56604, #93319 ) ) ;
#91444=ADVANCED_FACE ( 'NONE', ( #72387 ), #14520, .T. ) ;
#91445=CARTESIAN_POINT ( 'NONE',  ( -6.888417027594036846, 19.07602104198033643, -1.500000000000002220 ) ) ;
#91446=B_SPLINE_CURVE_WITH_KNOTS ( 'NONE', 3,
 ( #25704, #56178, #17093, #48569, #88118, #87104 ),
 .UNSPECIFIED., .F., .F.,
 ( 4, 2, 4 ),
 ( 0.000000000000000000, 0.001380901958385395483, 0.002761803916770790967 ),
 .UNSPECIFIED. ) ;
#91447=CARTESIAN_POINT ( 'NONE',  ( -69.83931149620484291, -25.31531697701531769, 4.914945103882936372 ) ) ;
#91451=EDGE_CURVE ( 'NONE', #81045, #38437, #15210, .T. ) ;
#91452=ORIENTED_EDGE ( 'NONE', *, *, #51547, .T. ) ;
#91453=CARTESIAN_POINT ( 'NONE',  ( -81.52287095715006160, -29.50248528299804818, 1.056150453629038477 ) ) ;
#91454=CARTESIAN_POINT ( 'NONE',  ( -62.22287095715008576, -23.47596703998600276, 11.44779298504227683 ) ) ;
#91455=CARTESIAN_POINT ( 'NONE',  ( 19.67429046578372365, -4.105084037421226739, -1.500000000000002220 ) ) ;
#91456=EDGE_CURVE ( 'NONE', #62727, #4330, #58708, .T. ) ;
#91457=CARTESIAN_POINT ( 'NONE',  ( -8.945158345017247825, -19.07159632999312393, 11.49999999999999645 ) ) ;
#91460=CARTESIAN_POINT ( 'NONE',  ( -21.51168160490077952, -5.175097382202364926, 11.49999999999998934 ) ) ;
#91461=EDGE_CURVE ( 'NONE', #30931, #5385, #28700, .T. ) ;
#91462=CARTESIAN_POINT ( 'NONE',  ( 20.13950599927006735, 4.067174238878714654, 11.49999999999998934 ) ) ;
#91463=B_SPLINE_CURVE_WITH_KNOTS ( 'NONE', 3,
 ( #67575, #5656, #59455, #7656 ),
 .UNSPECIFIED., .F., .F.,
 ( 4, 4 ),
 ( 0.03697762237835398869, 0.06648419838821313654 ),
 .UNSPECIFIED. ) ;
#91465=CARTESIAN_POINT ( 'NONE',  ( -60.66488206965777863, -23.48783264082476308, -1.443836473390097686 ) ) ;
#91466=ORIENTED_EDGE ( 'NONE', *, *, #59915, .T. ) ;
#91467=PLANE ( 'NONE',  #68717 ) ;
#91468=ORIENTED_EDGE ( 'NONE', *, *, #72066, .T. ) ;
#91469=CARTESIAN_POINT ( 'NONE',  ( -35.52287095715008292, -24.15516710230293640, 10.28746687063726561 ) ) ;
#91470=B_SPLINE_SURFACE_WITH_KNOTS ( 'NONE', 3, 3, ( 
 ( #8510, #55201, #1409, #1907 ),
 ( #31342, #32343, #63319, #94237 ),
 ( #69410, #24722, #77998, #55703 ),
 ( #48083, #25226, #79009, #54201 ),
 ( #54693, #40467, #63826, #23723 ),
 ( #71416, #38952, #100327, #32850 ),
 ( #23216, #94739, #56204, #62308 ),
 ( #17622, #85125, #48594, #7503 ),
 ( #15611, #77502, #93233, #16112 ),
 ( #39461, #70411, #897, #58684 ) ),
 .UNSPECIFIED., .F., .F., .F.,
 ( 4, 3, 3, 4 ),
 ( 4, 4 ),
 ( 0.0004766839783821102895, 0.1491231665100173909, 0.2234464077758350209, 0.2977696490416526509 ),
 ( 0.5495603723122651774, 0.5509005773147922502 ),
 .UNSPECIFIED. ) ;
#91475=CARTESIAN_POINT ( 'NONE',  ( -95.52287095715011844, -23.48783264082477373, -1.443836473390086139 ) ) ;
#91478=CARTESIAN_POINT ( 'NONE',  ( -7.851838630353038972, -19.11370409007043847, -1.500000000000002220 ) ) ;
#91479=CARTESIAN_POINT ( 'NONE',  ( -20.67203406374276398, -6.343553224398504220, 11.49999999999999645 ) ) ;
#91480=ORIENTED_EDGE ( 'NONE', *, *, #41302, .F. ) ;
#91481=CARTESIAN_POINT ( 'NONE',  ( -56.55620429048339304, -24.66019654487199020, 8.947790411086133489 ) ) ;
#91483=CARTESIAN_POINT ( 'NONE',  ( 12.52526618502215250, 18.50471055633022388, 11.49999999999998934 ) ) ;
#91484=CARTESIAN_POINT ( 'NONE',  ( -79.68206046389329344, -25.12205741196211051, 6.776761561512239851 ) ) ;
#91485=CARTESIAN_POINT ( 'NONE',  ( -61.52287095715006160, -24.64898659630367916, 1.056161002820822592 ) ) ;
#91486=ORIENTED_EDGE ( 'NONE', *, *, #35464, .F. ) ;
#91487=CARTESIAN_POINT ( 'NONE',  ( -43.58953762381672448, -23.47593901973091235, -1.443836447539011525 ) ) ;
#91488=CARTESIAN_POINT ( 'NONE',  ( -49.53586925223535076, -24.51419770103158413, 9.386484678747189392 ) ) ;
#91489=CARTESIAN_POINT ( 'NONE',  ( -19.40664508603899563, 7.695215611089875729, 11.49999999999998934 ) ) ;
#91490=ORIENTED_EDGE ( 'NONE', *, *, #22814, .T. ) ;
#91492=CARTESIAN_POINT ( 'NONE',  ( -86.52215078430889150, -23.48783264082478084, -1.443836473390066377 ) ) ;
#91494=B_SPLINE_CURVE_WITH_KNOTS ( 'NONE', 3,
 ( #61557, #22950, #46824, #84871, #69660, #137 ),
 .UNSPECIFIED., .F., .F.,
 ( 4, 2, 4 ),
 ( 0.000000000000000000, 0.001380764517853250986, 0.002761529035706501971 ),
 .UNSPECIFIED. ) ;
#91496=CARTESIAN_POINT ( 'NONE',  ( -109.5167357964235322, -24.15620529776628445, 10.23563542870660115 ) ) ;
#91497=CARTESIAN_POINT ( 'NONE',  ( 19.39439428382967634, -8.317090367284466268, -1.500000000000002220 ) ) ;
#91499=CARTESIAN_POINT ( 'NONE',  ( -112.5228709571500332, -24.50321055353805377, 9.387540953477518713 ) ) ;
#91500=CARTESIAN_POINT ( 'NONE',  ( -100.1979988280279201, -25.26221314647534300, 7.085054734328950943 ) ) ;
#91501=CARTESIAN_POINT ( 'NONE',  ( -19.96617879207914825, 8.700599545123990808, 11.49999999999998934 ) ) ;
#91502=LINE ( 'NONE', #98113, #95137 ) ;
#91503=CARTESIAN_POINT ( 'NONE',  ( -35.55620429048340014, -24.99156044556202261, 7.747789690856173195 ) ) ;
#91504=CARTESIAN_POINT ( 'NONE',  ( -80.18909136271707894, -25.13912158888506099, 7.067238146532562659 ) ) ;
#91505=CARTESIAN_POINT ( 'NONE',  ( 1.937016913031804455, -21.67664703184077268, -1.500000000000002220 ) ) ;
#91506=CARTESIAN_POINT ( 'NONE',  ( -78.95132930790050807, -25.25821045354187078, 6.187260761811991472 ) ) ;
#91507=CARTESIAN_POINT ( 'NONE',  ( 12.52526618502215250, 18.50471055633022388, 11.49999999999999645 ) ) ;
#91510=CARTESIAN_POINT ( 'NONE',  ( -85.58094713038467205, -25.00182538069147142, 7.747789668545045139 ) ) ;
#91511=EDGE_CURVE ( 'NONE', #31248, #64842, #94997, .T. ) ;
#91512=B_SPLINE_CURVE_WITH_KNOTS ( 'NONE', 3,
 ( #1508, #32444, #24824, #71520, #25830, #37671 ),
 .UNSPECIFIED., .F., .F.,
 ( 4, 2, 4 ),
 ( 0.000000000000000000, 0.001380764517854760412, 0.002761529035709520824 ),
 .UNSPECIFIED. ) ;
#91515=AXIS2_PLACEMENT_3D ( 'NONE', #24241, #54709, #1420 ) ;
#91516=B_SPLINE_CURVE_WITH_KNOTS ( 'NONE', 3,
 ( #32167, #94067, #48411, #70239 ),
 .UNSPECIFIED., .F., .F.,
 ( 4, 4 ),
 ( 6.938893903907227607E-18, 9.999999999999593903E-05 ),
 .UNSPECIFIED. ) ;
#91519=B_SPLINE_CURVE_WITH_KNOTS ( 'NONE', 3,
 ( #84681, #54253, #85183, #15672, #8062, #18176 ),
 .UNSPECIFIED., .F., .F.,
 ( 4, 2, 4 ),
 ( 1.570755371633915156E-05, 0.001396183895866086452, 0.002776660238015833844 ),
 .UNSPECIFIED. ) ;
#91522=CARTESIAN_POINT ( 'NONE',  ( -10.79823215447539653, -18.26288818932900071, 11.49999999999998934 ) ) ;
#91523=LINE ( 'NONE', #67716, #2803 ) ;
#91524=CARTESIAN_POINT ( 'NONE',  ( -79.10019335338344604, -25.03138112166652007, 6.701029380949082181 ) ) ;
#91525=CARTESIAN_POINT ( 'NONE',  ( -63.52287095715006160, -29.50250243563736774, 8.947779886222145151 ) ) ;
#91527=CARTESIAN_POINT ( 'NONE',  ( -1.480291460309441920, -19.30061035156251847, -1.500000000000002220 ) ) ;
#91529=CARTESIAN_POINT ( 'NONE',  ( -51.89024320248035593, -25.28679719141751647, 5.841385604566403877 ) ) ;
#91531=CARTESIAN_POINT ( 'NONE',  ( -4.672984603565591755, -18.88948546680484242, 11.49999999999999645 ) ) ;
#91533=EDGE_CURVE ( 'NONE', #80499, #33585, #50537, .T. ) ;
#91537=DIRECTION ( 'NONE',  ( 0.000000000000000000, 0.9999999999976377785, 2.173523156925979975E-06 ) ) ;
#91538=DIRECTION ( 'NONE',  ( 0.000000000000000000, -0.8403332392196035672, 0.5420701495772373146 ) ) ;
#91539=CARTESIAN_POINT ( 'NONE',  ( 9.307004028210867475, 17.29072351678862418, 11.49999999999998934 ) ) ;
#91541=VERTEX_POINT ( 'NONE', #57662 ) ;
#91542=AXIS2_PLACEMENT_3D ( 'NONE', #71735, #65142, #89450 ) ;
#91543=CARTESIAN_POINT ( 'NONE',  ( 10.28227983848843152, -18.94921665015282031, -1.500000000000002220 ) ) ;
#91545=CARTESIAN_POINT ( 'NONE',  ( -70.78633892220865675, -25.25639579675769752, 7.001279323389742792 ) ) ;
#91546=CARTESIAN_POINT ( 'NONE',  ( -43.52287095715004739, -23.48783264083374078, -1.443836473376152840 ) ) ;
#91547=CARTESIAN_POINT ( 'NONE',  ( -99.62727860833967952, -25.18439417509214096, 3.670122307788938887 ) ) ;
#91548=CARTESIAN_POINT ( 'NONE',  ( 18.43541038833219758, -13.85303862407246811, -1.500000000000002220 ) ) ;
#91551=CARTESIAN_POINT ( 'NONE',  ( -93.59138681930647863, -24.15543982623907482, -0.2315651400026620677 ) ) ;
#91552=CARTESIAN_POINT ( 'NONE',  ( -49.48509645508600840, -24.65952944569304606, 1.056160979905696129 ) ) ;
#91553=CARTESIAN_POINT ( 'NONE',  ( 16.68447708738676383, -11.30049470069299922, 11.49999999999999645 ) ) ;
#91554=CARTESIAN_POINT ( 'NONE',  ( -45.62287095715004881, -24.14406661707768720, 10.28769366152059739 ) ) ;
#91555=DIRECTION ( 'NONE',  ( 0.000000000000000000, -2.173523156925979552E-06, 0.9999999999976378895 ) ) ;
#91556=CARTESIAN_POINT ( 'NONE',  ( -94.55620429048340725, -23.48786465467241413, 11.44779295918254647 ) ) ;
#91558=CARTESIAN_POINT ( 'NONE',  ( -110.4389802415574309, -25.29779155955683478, 3.296667605415470881 ) ) ;
#91559=CARTESIAN_POINT ( 'NONE',  ( 11.24879072547334324, 16.40116332625411033, -1.500000000000002220 ) ) ;
#91561=CARTESIAN_POINT ( 'NONE',  ( -16.30015253881794379, -11.17962500214296639, -1.500000000000002220 ) ) ;
#91562=CARTESIAN_POINT ( 'NONE',  ( -126.5891254613743797, -24.66019654487200796, 8.947790411086103290 ) ) ;
#91565=CARTESIAN_POINT ( 'NONE',  ( 20.68991284688621946, 0.5745778482356619365, 11.49999999999999645 ) ) ;
#91569=CARTESIAN_POINT ( 'NONE',  ( -50.26765004257320868, -25.25138673217113094, 5.200244656635645946 ) ) ;
#91570=CARTESIAN_POINT ( 'NONE',  ( 13.52301212282245935, 18.22803923376396540, 11.49999999999999645 ) ) ;
#91573=CARTESIAN_POINT ( 'NONE',  ( -70.32380231474228083, -25.12298712672050982, 7.101635559041870494 ) ) ;
#91574=CARTESIAN_POINT ( 'NONE',  ( -12.46103870137906711, 15.87156016069071462, 11.49999999999998934 ) ) ;
#91575=ADVANCED_FACE ( 'NONE', ( #80988 ), #20078, .F. ) ;
#91578=CARTESIAN_POINT ( 'NONE',  ( -41.40661852069504079, -25.29534531538531894, 4.500433469842812784 ) ) ;
#91579=ORIENTED_EDGE ( 'NONE', *, *, #65277, .T. ) ;
#91580=AXIS2_PLACEMENT_3D ( 'NONE', #46302, #85868, #70641 ) ;
#91582=DIRECTION ( 'NONE',  ( 1.000000000000000000, 3.773278334444167608E-23, 8.201307833595939069E-29 ) ) ;
#91583=CARTESIAN_POINT ( 'NONE',  ( -17.51315278866654879, 14.73147661606379621, -1.500000000000002220 ) ) ;
#91584=CARTESIAN_POINT ( 'NONE',  ( -111.3711097089617965, -25.28332809916757640, 4.263977541267919058 ) ) ;
#91585=CARTESIAN_POINT ( 'NONE',  ( 16.85579979752674618, 13.57973486276658903, -1.500000000000002220 ) ) ;
#91586=CARTESIAN_POINT ( 'NONE',  ( -30.57287095715006942, -23.48213395187224606, 11.44779283644488999 ) ) ;
#91587=CARTESIAN_POINT ( 'NONE',  ( -114.6228709571500559, -23.47593901973091235, -1.443836447538999312 ) ) ;
#91589=CARTESIAN_POINT ( 'NONE',  ( -9.975069251262826953, -18.38325097723136992, 11.49999999999999645 ) ) ;
#91591=CARTESIAN_POINT ( 'NONE',  ( -87.22287095715009286, -23.47593901973090880, -1.443836447538997314 ) ) ;
#91592=CARTESIAN_POINT ( 'NONE',  ( -4.682628417673765142, 21.48327871026360114, 11.49999999999998934 ) ) ;
#91594=CARTESIAN_POINT ( 'NONE',  ( -105.5497123930152270, -24.63419186844610920, 9.035850630976920428 ) ) ;
#91595=CARTESIAN_POINT ( 'NONE',  ( -41.86772617331516955, -25.29087320296346775, 4.147750017007223455 ) ) ;
#91596=ORIENTED_EDGE ( 'NONE', *, *, #68767, .F. ) ;
#91597=CARTESIAN_POINT ( 'NONE',  ( -73.58953762381672448, -23.47593901973091235, -1.443836447539006196 ) ) ;
#91598=DIRECTION ( 'NONE',  ( 1.000000000000000000, 3.773278334444167608E-23, 8.201307833595939069E-29 ) ) ;
#91599=ORIENTED_EDGE ( 'NONE', *, *, #19087, .T. ) ;
#91601=ORIENTED_EDGE ( 'NONE', *, *, #30538, .F. ) ;
#91602=ORIENTED_EDGE ( 'NONE', *, *, #19862, .F. ) ;
#91604=CARTESIAN_POINT ( 'NONE',  ( -101.5937515207030657, -25.10935946579351352, 3.495447590598027787 ) ) ;
#91605=CARTESIAN_POINT ( 'NONE',  ( -102.9228709571500957, -23.47593901973090524, -1.443836447538997314 ) ) ;
#91606=ADVANCED_FACE ( 'NONE', ( #15949 ), #45926, .T. ) ;
#91607=CARTESIAN_POINT ( 'NONE',  ( 12.15263457413992576, -16.39098610538439615, -1.500000000000002220 ) ) ;
#91608=ORIENTED_EDGE ( 'NONE', *, *, #99905, .F. ) ;
#91610=CARTESIAN_POINT ( 'NONE',  ( -30.63234162661936111, -23.86952536761622667, -1.017619990082605952 ) ) ;
#91611=LINE ( 'NONE', #92113, #52942 ) ;
#91612=LINE ( 'NONE', #6882, #69111 ) ;
#91615=CARTESIAN_POINT ( 'NONE',  ( -29.74590468580106872, -24.63645583638522751, 6.038517363561788365 ) ) ;
#91617=CARTESIAN_POINT ( 'NONE',  ( 17.70469293622815243, 10.90570606759641592, -1.500000000000002220 ) ) ;
#91619=CARTESIAN_POINT ( 'NONE',  ( -106.6228709571500559, -24.66019654487199730, 8.947790411086122830 ) ) ;
#91620=ORIENTED_EDGE ( 'NONE', *, *, #6075, .T. ) ;
#91621=CARTESIAN_POINT ( 'NONE',  ( -28.62287095715005947, -24.18537418825495777, 9.819270430423445717 ) ) ;
#91623=VERTEX_POINT ( 'NONE', #23559 ) ;
#91625=CARTESIAN_POINT ( 'NONE',  ( -92.62287095715005592, -24.35013146730204170, 9.818937971375108376 ) ) ;
#91626=CARTESIAN_POINT ( 'NONE',  ( -60.62287095715004881, -23.47596703998600631, 11.44779298504227505 ) ) ;
#91627=CARTESIAN_POINT ( 'NONE',  ( -100.5925999562403490, -25.25419553508370285, 7.559861005836696179 ) ) ;
#91630=CARTESIAN_POINT ( 'NONE',  ( 4.260453091581613450, -21.75001586557718980, 11.49999999999999645 ) ) ;
#91631=VERTEX_POINT ( 'NONE', #54042 ) ;
#91633=CARTESIAN_POINT ( 'NONE',  ( 3.867644355387967359, 22.30990608135428488, 11.49999999999998934 ) ) ;
#91637=B_SPLINE_CURVE_WITH_KNOTS ( 'NONE', 3,
 ( #9234, #85869, #70140, #86858, #95481, #32074 ),
 .UNSPECIFIED., .F., .F.,
 ( 4, 2, 4 ),
 ( 0.000000000000000000, 0.001380901958385393315, 0.002761803916770786630 ),
 .UNSPECIFIED. ) ;
#91638=ORIENTED_EDGE ( 'NONE', *, *, #9576, .F. ) ;
#91641=AXIS2_PLACEMENT_3D ( 'NONE', #34828, #96715, #27216 ) ;
#91642=B_SPLINE_CURVE_WITH_KNOTS ( 'NONE', 3,
 ( #17968, #87476, #48928, #87984 ),
 .UNSPECIFIED., .F., .F.,
 ( 4, 4 ),
 ( 0.7393053958805789749, 0.7403061429213444455 ),
 .UNSPECIFIED. ) ;
#91643=CARTESIAN_POINT ( 'NONE',  ( 1.915021276000606454, 20.04344799065331628, 11.49999999999998934 ) ) ;
#91647=CARTESIAN_POINT ( 'NONE',  ( 19.44376294880228428, 11.01865886811674677, -1.500000000000002220 ) ) ;
#91650=VERTEX_POINT ( 'NONE', #62152 ) ;
#91653=CARTESIAN_POINT ( 'NONE',  ( -80.93694966678978631, -25.04514726203225550, 7.505594008164218067 ) ) ;
#91655=FACE_OUTER_BOUND ( 'NONE', #89102, .T. ) ;
#91658=CARTESIAN_POINT ( 'NONE',  ( -12.10551386448753064, 15.32171617432465816, 11.49999999999998934 ) ) ;
#91659=CARTESIAN_POINT ( 'NONE',  ( -47.52287095715004739, -24.34917612407052090, 0.1852690917482640864 ) ) ;
#91660=CARTESIAN_POINT ( 'NONE',  ( 7.480126432006339421, -20.11416664461015458, -1.500000000000002220 ) ) ;
#91662=CARTESIAN_POINT ( 'NONE',  ( -111.5228709571500616, -29.50248528299804818, 1.056150453629043584 ) ) ;
#91663=CARTESIAN_POINT ( 'NONE',  ( -111.3776484685884185, -25.28710546256126079, 4.332404433089555695 ) ) ;
#91664=CARTESIAN_POINT ( 'NONE',  ( 9.198035947750891950, -20.93187084735588144, -1.500000000000002220 ) ) ;
#91665=EDGE_CURVE ( 'NONE', #62568, #21835, #99676, .T. ) ;
#91666=CARTESIAN_POINT ( 'NONE',  ( -106.6300409130544580, -23.96169478059714564, 10.65365249895717170 ) ) ;
#91667=DIRECTION ( 'NONE',  ( 0.000000000000000000, 2.173523156925980399E-06, -0.9999999999976378895 ) ) ;
#91668=CARTESIAN_POINT ( 'NONE',  ( 0.05828707793547563409, -19.95834144014285272, 11.49999999999999645 ) ) ;
#91669=CARTESIAN_POINT ( 'NONE',  ( -50.52287095715005449, -24.92579138211018019, 1.929029949965659352 ) ) ;
#91670=PLANE ( 'NONE',  #13291 ) ;
#91671=CARTESIAN_POINT ( 'NONE',  ( -44.52287095715006160, -23.47593901973090169, -1.443836447538997092 ) ) ;
#91672=VERTEX_POINT ( 'NONE', #76837 ) ;
#91673=CARTESIAN_POINT ( 'NONE',  ( -83.52287095715009002, -24.35013146730203815, 9.818937971375104823 ) ) ;
#91674=CARTESIAN_POINT ( 'NONE',  ( -52.62287095715004170, -23.47596703998600276, 11.44779298504227505 ) ) ;
#91675=CARTESIAN_POINT ( 'NONE',  ( -16.45766974254678061, 14.19212061201335473, 11.49999999999998934 ) ) ;
#91678=CARTESIAN_POINT ( 'NONE',  ( 3.528372621398383924, 19.26332229581237598, -1.500000000000002220 ) ) ;
#91679=CARTESIAN_POINT ( 'NONE',  ( -99.96323870662324396, -25.14579874352854816, 7.028128672497866880 ) ) ;
#91684=CARTESIAN_POINT ( 'NONE',  ( -13.28352777634190396, 15.58691228024164310, 11.49999999999999645 ) ) ;
#91691=CARTESIAN_POINT ( 'NONE',  ( -69.34303308397305443, -25.25559839591755207, 6.209207386190695566 ) ) ;
#91692=ADVANCED_FACE ( 'NONE', ( #38294 ), #77345, .T. ) ;
#91693=CARTESIAN_POINT ( 'NONE',  ( -61.62287095715002749, -23.72747288104441665, -1.053458166803662666 ) ) ;
#91695=VECTOR ( 'NONE', #84568, 1000.000000000000114 ) ;
#91696=CARTESIAN_POINT ( 'NONE',  ( -5.126879528927636542, -22.49243673399587351, 11.49999999999999645 ) ) ;
#91697=CARTESIAN_POINT ( 'NONE',  ( 20.43669262517703800, -10.12641136740851699, 11.49999999999998934 ) ) ;
#91699=CARTESIAN_POINT ( 'NONE',  ( -28.62287095715004881, -24.49608681932686949, 1.056161686216224860 ) ) ;
#91700=CARTESIAN_POINT ( 'NONE',  ( -63.92287095715007439, -23.47593901973090524, -1.443836447538998202 ) ) ;
#91701=DIRECTION ( 'NONE',  ( 1.000000000000000000, 3.773278334444166432E-23, 8.201307841325785021E-29 ) ) ;
#91702=CARTESIAN_POINT ( 'NONE',  ( -110.5895385589013955, -24.52300882791530512, 0.6510814631126382590 ) ) ;
#91703=CARTESIAN_POINT ( 'NONE',  ( 20.64021973274467570, 7.317367941133321452, 11.49999999999998934 ) ) ;
#91705=CARTESIAN_POINT ( 'NONE',  ( -43.62287095715004881, -24.65952944569304606, 1.056160979905692576 ) ) ;
#91707=CARTESIAN_POINT ( 'NONE',  ( -50.62287095715006302, -24.63287334234178871, 0.9662140553045418523 ) ) ;
#91711=LINE ( 'NONE', #37936, #93822 ) ;
#91712=DIRECTION ( 'NONE',  ( -0.000000000000000000, 2.173523156925979552E-06, -0.9999999999976378895 ) ) ;
#91715=CARTESIAN_POINT ( 'NONE',  ( 5.749347661499963458, 19.61174949527739386, -1.500000000000002220 ) ) ;
#91716=ORIENTED_EDGE ( 'NONE', *, *, #63941, .F. ) ;
#91718=VERTEX_POINT ( 'NONE', #16957 ) ;
#91719=ORIENTED_EDGE ( 'NONE', *, *, #6148, .F. ) ;
#91720=VERTEX_POINT ( 'NONE', #87983 ) ;
#91721=CARTESIAN_POINT ( 'NONE',  ( -3.733506833432379768, 22.73668382284982314, -1.500000000000002220 ) ) ;
#91723=EDGE_CURVE ( 'NONE', #88666, #22199, #17544, .T. ) ;
#91724=CARTESIAN_POINT ( 'NONE',  ( 8.375906630400100639, -18.44307005126401933, -1.500000000000002220 ) ) ;
#91727=CARTESIAN_POINT ( 'NONE',  ( -29.26545924526617881, -25.19927926512142591, 4.027978703335532096 ) ) ;
#91728=CARTESIAN_POINT ( 'NONE',  ( -87.62287095715011276, -24.35013146730204525, 9.818937971375108376 ) ) ;
#91730=ADVANCED_FACE ( 'NONE', ( #734 ), #95588, .F. ) ;
#91731=CARTESIAN_POINT ( 'NONE',  ( -51.62287095715005592, -24.64965695001468404, 8.947790433994185832 ) ) ;
#91732=CARTESIAN_POINT ( 'NONE',  ( -70.64339238044932756, -24.15503026093916006, -0.2815557561904372674 ) ) ;
#91733=CARTESIAN_POINT ( 'NONE',  ( 21.23773461148298836, -3.020459416520930862, 11.49999999999999645 ) ) ;
#91734=ORIENTED_EDGE ( 'NONE', *, *, #42286, .T. ) ;
#91735=DIRECTION ( 'NONE',  ( -3.773278334453079030E-23, 0.9999999999976377785, 2.173523156925979128E-06 ) ) ;
#91736=CARTESIAN_POINT ( 'NONE',  ( -61.64238508986091603, -23.96169478059713143, 10.65365249895718591 ) ) ;
#91738=CARTESIAN_POINT ( 'NONE',  ( -6.500255983836059848, -19.66680810221124887, -1.500000000000002220 ) ) ;
#91740=ORIENTED_EDGE ( 'NONE', *, *, #53796, .F. ) ;
#91744=ORIENTED_EDGE ( 'NONE', *, *, #32145, .F. ) ;
#91746=CARTESIAN_POINT ( 'NONE',  ( 0.1985894851802381678, 21.93841921393417849, 11.49999999999999645 ) ) ;
#91747=CARTESIAN_POINT ( 'NONE',  ( -37.64896865082437216, -23.96169478059712432, 10.65365249895718591 ) ) ;
#91748=CARTESIAN_POINT ( 'NONE',  ( 22.54279463279464579, 0.6884863543687869125, 11.49999999999998934 ) ) ;
#91750=CARTESIAN_POINT ( 'NONE',  ( -18.08314111433443827, -10.61732331186343004, -1.500000000000002220 ) ) ;
#91751=CARTESIAN_POINT ( 'NONE',  ( -108.9545715455114987, -25.28708312187852414, 4.170144817753115518 ) ) ;
#91752=CARTESIAN_POINT ( 'NONE',  ( -53.52287095715006870, -23.48786465467241058, 11.44779295918255002 ) ) ;
#91753=VERTEX_POINT ( 'NONE', #39795 ) ;
#91755=ORIENTED_EDGE ( 'NONE', *, *, #6045, .F. ) ;
#91756=CARTESIAN_POINT ( 'NONE',  ( -66.64657122283996671, -23.73766607897669800, -1.055555164236460897 ) ) ;
#91757=CARTESIAN_POINT ( 'NONE',  ( 18.51311748589099082, 11.02308708543723270, -1.500000000000002220 ) ) ;
#91761=CARTESIAN_POINT ( 'NONE',  ( -2.902382693073098707, -20.91247731031871382, -1.500000000000002220 ) ) ;
#91762=CARTESIAN_POINT ( 'NONE',  ( -126.6228709571499991, -23.96127896941632685, -0.6493128931037731588 ) ) ;
#91764=CARTESIAN_POINT ( 'NONE',  ( -100.5228709571500332, -24.15431212366390668, -0.2830839119429366946 ) ) ;
#91766=DIRECTION ( 'NONE',  ( 1.000000000000000000, 2.567145104884906770E-18, 5.579749332669698856E-24 ) ) ;
#91767=CARTESIAN_POINT ( 'NONE',  ( -12.04397493737346991, 18.63154960201688226, -1.500000000000002220 ) ) ;
#91768=CARTESIAN_POINT ( 'NONE',  ( -71.58791429090274505, -24.34968618360933945, 0.1864209137778822800 ) ) ;
#91770=CARTESIAN_POINT ( 'NONE',  ( -82.52287095715006160, -23.47596703998600631, 11.44779298504228571 ) ) ;
#91771=CARTESIAN_POINT ( 'NONE',  ( -33.62287095715005592, -23.47593901973091235, -1.443836447539013301 ) ) ;
#91775=CARTESIAN_POINT ( 'NONE',  ( -17.86923650574433609, -7.721772263035739492, 11.49999999999998934 ) ) ;
#91776=CARTESIAN_POINT ( 'NONE',  ( -11.99125074976391048, 17.70416384622758343, -1.500000000000002220 ) ) ;
#91777=CARTESIAN_POINT ( 'NONE',  ( -62.56626437149660802, -23.48783264082476308, -1.443836473390090580 ) ) ;
#91778=B_SPLINE_CURVE_WITH_KNOTS ( 'NONE', 3,
 ( #48355, #80800, #34630, #86900, #65599, #17898, #27011, #88916 ),
 .UNSPECIFIED., .F., .F.,
 ( 4, 2, 2, 4 ),
 ( -0.001224873891641428247, -0.0002244903592271104472, 0.0007758931731872069186, 0.002776660238015841217 ),
 .UNSPECIFIED. ) ;
#91779=CARTESIAN_POINT ( 'NONE',  ( -106.5228709571500332, -23.48783264082477018, -1.443836473390085695 ) ) ;
#91780=B_SPLINE_CURVE_WITH_KNOTS ( 'NONE', 3,
 ( #94295, #1970, #48145, #9566 ),
 .UNSPECIFIED., .F., .F.,
 ( 4, 4 ),
 ( 0.3400287306710966240, 0.3490351619432120467 ),
 .UNSPECIFIED. ) ;
#91781=CARTESIAN_POINT ( 'NONE',  ( -123.5228709571500474, -23.94994826722565406, -0.6494450866342700301 ) ) ;
#91782=DIRECTION ( 'NONE',  ( -3.773278334453079030E-23, 0.9999999999976377785, 2.173523156925979128E-06 ) ) ;
#91783=CARTESIAN_POINT ( 'NONE',  ( -12.01393383709116947, -19.22582291892495121, -1.500000000000002220 ) ) ;
#91784=VECTOR ( 'NONE', #64514, 1000.000000000000114 ) ;
#91785=EDGE_CURVE ( 'NONE', #38852, #16349, #43088, .T. ) ;
#91786=ORIENTED_EDGE ( 'NONE', *, *, #45422, .F. ) ;
#91788=DIRECTION ( 'NONE',  ( -3.773278334453079618E-23, 0.9999999999976377785, 2.173523156925979975E-06 ) ) ;
#91789=FACE_OUTER_BOUND ( 'NONE', #66310, .T. ) ;
#91790=CARTESIAN_POINT ( 'NONE',  ( -18.99895575154661742, -5.639348582513488140, 11.49999999999999645 ) ) ;
#91793=DIRECTION ( 'NONE',  ( -1.000000000000000000, -3.773278334444166432E-23, -8.201307841325785021E-29 ) ) ;
#91794=ORIENTED_EDGE ( 'NONE', *, *, #8182, .T. ) ;
#91795=CARTESIAN_POINT ( 'NONE',  ( -68.62287095715004170, -24.66019654487199020, 8.947790411086131712 ) ) ;
#91796=DIRECTION ( 'NONE',  ( -3.773278334453079618E-23, 0.9999999999976377785, 2.173523156925979975E-06 ) ) ;
#91797=EDGE_CURVE ( 'NONE', #94885, #12627, #86555, .T. ) ;
#91798=CARTESIAN_POINT ( 'NONE',  ( -10.14273968512601520, 19.10955606681249463, 11.49999999999998934 ) ) ;
#91800=CARTESIAN_POINT ( 'NONE',  ( -49.59577668750772972, -25.10935179600810230, 3.074246299446597774 ) ) ;
#91801=CARTESIAN_POINT ( 'NONE',  ( 11.34002819025610087, 15.78594478779102950, -1.500000000000002220 ) ) ;
#91802=AXIS2_PLACEMENT_3D ( 'NONE', #5347, #44420, #44920 ) ;
#91804=EDGE_CURVE ( 'NONE', #14758, #5846, #99834, .T. ) ;
#91805=CARTESIAN_POINT ( 'NONE',  ( -82.52287095715004739, -24.35013146730204525, 9.818937971375101270 ) ) ;
#91807=CARTESIAN_POINT ( 'NONE',  ( 18.95923836289803788, 5.684714004613049987, -1.500000000000002220 ) ) ;
#91808=ORIENTED_EDGE ( 'NONE', *, *, #82881, .F. ) ;
#91809=EDGE_CURVE ( 'NONE', #908, #44968, #62654, .T. ) ;
#91810=CARTESIAN_POINT ( 'NONE',  ( 11.02309159617336221, -17.05227643984133934, 11.49999999999999645 ) ) ;
#91811=CARTESIAN_POINT ( 'NONE',  ( -80.60234417792803185, -23.85016227208580020, -0.8807180028928338622 ) ) ;
#91814=CARTESIAN_POINT ( 'NONE',  ( -102.5221944888360497, -23.48786465467241058, 11.44779295918254292 ) ) ;
#91815=CARTESIAN_POINT ( 'NONE',  ( -119.4728709594060376, -25.40676080801054937, 8.000950335809053016 ) ) ;
#91816=CARTESIAN_POINT ( 'NONE',  ( -96.62287095715005592, -24.50321055353805377, 9.387540953477525818 ) ) ;
#91817=CARTESIAN_POINT ( 'NONE',  ( -40.65333657091576924, -24.15602025860895097, 10.28564288303536856 ) ) ;
#91818=CARTESIAN_POINT ( 'NONE',  ( -108.5228709571500616, -29.50248528299804818, 1.056150453629043584 ) ) ;
#91819=CARTESIAN_POINT ( 'NONE',  ( -16.95507112718987486, -10.73317591066004084, 11.49999999999998934 ) ) ;
#91821=EDGE_CURVE ( 'NONE', #99101, #84023, #74522, .T. ) ;
#91823=ORIENTED_EDGE ( 'NONE', *, *, #34556, .T. ) ;
#91824=CARTESIAN_POINT ( 'NONE',  ( -129.6228709571500417, -23.47593901973091235, -1.443836447538995760 ) ) ;
#91826=CARTESIAN_POINT ( 'NONE',  ( 22.81499323874321661, -2.031749852351878882, 11.49999999999999645 ) ) ;
#91827=CARTESIAN_POINT ( 'NONE',  ( 4.564784964189898098, -22.25151590922551748, -1.500000000000002220 ) ) ;
#91830=CARTESIAN_POINT ( 'NONE',  ( -38.64173386164763713, -24.15620529776627379, 10.23563542870660825 ) ) ;
#91832=CARTESIAN_POINT ( 'NONE',  ( -43.55620429048340014, -24.64965694238574656, 8.947790433994203596 ) ) ;
#91834=CARTESIAN_POINT ( 'NONE',  ( -32.22287095715005023, -23.47593901973090169, -1.443836447538997980 ) ) ;
#91836=ORIENTED_EDGE ( 'NONE', *, *, #21970, .F. ) ;
#91837=CARTESIAN_POINT ( 'NONE',  ( -20.10423522397153562, 3.301153050299447056, -1.500000000000002220 ) ) ;
#91839=CARTESIAN_POINT ( 'NONE',  ( 14.22603995551189371, 18.00578905361294346, 11.49999999999998934 ) ) ;
#91841=CARTESIAN_POINT ( 'NONE',  ( -53.52287095715006160, -23.73934037231757088, 11.05740245334329153 ) ) ;
#91842=ORIENTED_EDGE ( 'NONE', *, *, #25952, .T. ) ;
#91843=CARTESIAN_POINT ( 'NONE',  ( -108.5907114367411879, -24.15620529776629155, 10.23563542870659404 ) ) ;
#91845=ADVANCED_FACE ( 'NONE', ( #71254 ), #41306, .T. ) ;
#91846=CARTESIAN_POINT ( 'NONE',  ( -77.62997961999919028, -24.35071581493544102, 9.817618358456021710 ) ) ;
#91848=CARTESIAN_POINT ( 'NONE',  ( -51.63317546500711330, -24.35071581493543036, 9.817618358456028815 ) ) ;
#91849=CARTESIAN_POINT ( 'NONE',  ( -1.624102159174229731, 21.17438964843747584, 11.49999999999999645 ) ) ;
#91852=CARTESIAN_POINT ( 'NONE',  ( 17.07819277939130842, -14.19623557145530057, 11.49999999999998934 ) ) ;
#91853=CARTESIAN_POINT ( 'NONE',  ( -16.41017380093149214, -12.48182641202616416, -1.500000000000002220 ) ) ;
#91858=CARTESIAN_POINT ( 'NONE',  ( -39.04644334225289271, -25.28415765582125729, 4.123731396711104225 ) ) ;
#91859=ORIENTED_EDGE ( 'NONE', *, *, #21145, .F. ) ;
#91861=CARTESIAN_POINT ( 'NONE',  ( -91.63120794989035289, -24.15543982623907837, -0.2315651400026614848 ) ) ;
#91862=AXIS2_PLACEMENT_3D ( 'NONE', #74663, #60466, #97008 ) ;
#91865=LINE ( 'NONE', #22336, #34139 ) ;
#91866=CARTESIAN_POINT ( 'NONE',  ( 20.57277012135545036, 3.371850554975475145, -1.500000000000002220 ) ) ;
#91867=CARTESIAN_POINT ( 'NONE',  ( 18.19902423439809525, 11.99547645517801442, 11.49999999999999645 ) ) ;
#91869=FACE_OUTER_BOUND ( 'NONE', #65931, .T. ) ;
#91870=CARTESIAN_POINT ( 'NONE',  ( 15.63351008929417318, -16.12541905121107177, 11.49999999999998934 ) ) ;
#91872=ORIENTED_EDGE ( 'NONE', *, *, #84034, .F. ) ;
#91877=CARTESIAN_POINT ( 'NONE',  ( -46.52204127861840277, -23.48786465467240703, 11.44779295918255180 ) ) ;
#91878=EDGE_LOOP ( 'NONE', ( #78239, #13970, #57070, #40217 ) ) ;
#91879=CARTESIAN_POINT ( 'NONE',  ( 18.88549913130557556, 9.949676122998861061, -1.500000000000002220 ) ) ;
#91880=EDGE_LOOP ( 'NONE', ( #81885, #36483, #43784, #5304 ) ) ;
#91881=CARTESIAN_POINT ( 'NONE',  ( -6.845587600281468177, 19.88882266644084496, -1.500000000000002220 ) ) ;
#91882=DIRECTION ( 'NONE',  ( -3.773278334444167608E-23, 1.000000000000000000, 0.000000000000000000 ) ) ;
#91883=CARTESIAN_POINT ( 'NONE',  ( -100.2189343329491464, -25.18669221479178333, 3.306178502990604340 ) ) ;
#91885=CARTESIAN_POINT ( 'NONE',  ( -15.43752342082821905, -15.63289427301443801, -1.500000000000002220 ) ) ;
#91886=CARTESIAN_POINT ( 'NONE',  ( -87.51796580416235827, -23.73766607897671932, -1.055555164236430032 ) ) ;
#91887=ORIENTED_EDGE ( 'NONE', *, *, #78875, .F. ) ;
#91888=CARTESIAN_POINT ( 'NONE',  ( -80.52287095715006160, -29.50248528299804818, 1.056150453629038477 ) ) ;
#91890=CARTESIAN_POINT ( 'NONE',  ( -84.58538098145766071, -24.51419770103157347, 9.386484678747175181 ) ) ;
#91891=B_SPLINE_CURVE_WITH_KNOTS ( 'NONE', 3,
 ( #13057, #75449, #37415, #66875, #99774, #99293 ),
 .UNSPECIFIED., .F., .F.,
 ( 4, 2, 4 ),
 ( 6.384118694783952546E-06, 0.001386860460836456845, 0.002767336802978129749 ),
 .UNSPECIFIED. ) ;
#91892=CARTESIAN_POINT ( 'NONE',  ( -128.5228709571501611, -24.34917612407044629, 0.1852690917480327160 ) ) ;
#91893=VECTOR ( 'NONE', #26658, 1000.000000000000114 ) ;
#91894=CARTESIAN_POINT ( 'NONE',  ( -10.25843596179259265, -22.80680519657271788, 9.703205396196688426 ) ) ;
#91895=CARTESIAN_POINT ( 'NONE',  ( 7.794017451908327843, -19.83292067980804774, 11.49999999999998934 ) ) ;
#91896=CARTESIAN_POINT ( 'NONE',  ( -98.63812701921389703, -23.48786465467241058, 11.44779295918254114 ) ) ;
#91897=CARTESIAN_POINT ( 'NONE',  ( -107.5944981716039024, -23.73791477778912196, 11.05961554403169700 ) ) ;
#91899=CARTESIAN_POINT ( 'NONE',  ( -33.62923966249122287, -24.51314013834315375, 0.6176544820404119562 ) ) ;
#91900=CARTESIAN_POINT ( 'NONE',  ( -18.88510386880526326, 12.19974334031638641, -1.500000000000002220 ) ) ;
#91901=EDGE_CURVE ( 'NONE', #85237, #53220, #88984, .T. ) ;
#91903=DIRECTION ( 'NONE',  ( 0.000000000000000000, 2.173523156925980399E-06, -0.9999999999976378895 ) ) ;
#91904=ORIENTED_EDGE ( 'NONE', *, *, #45911, .F. ) ;
#91905=EDGE_CURVE ( 'NONE', #11783, #21736, #33364, .T. ) ;
#91906=PLANE ( 'NONE',  #54717 ) ;
#91907=CARTESIAN_POINT ( 'NONE',  ( 0.9049686737998731134, -19.58615294826029540, 11.49999999999999645 ) ) ;
#91908=CARTESIAN_POINT ( 'NONE',  ( -72.62287095715005592, -29.50250786944525672, 11.44777988621623699 ) ) ;
#91909=EDGE_CURVE ( 'NONE', #52078, #62568, #56396, .T. ) ;
#91910=DIRECTION ( 'NONE',  ( -3.773278334444167608E-23, 1.000000000000000000, 0.000000000000000000 ) ) ;
#91912=EDGE_CURVE ( 'NONE', #98224, #73156, #90158, .T. ) ;
#91913=CARTESIAN_POINT ( 'NONE',  ( -50.62287095715004170, -23.48783264082478084, -1.443836473390070596 ) ) ;
#91914=CARTESIAN_POINT ( 'NONE',  ( -124.6623029623788312, -25.38371629874578161, 5.756521249355254000 ) ) ;
#91915=CARTESIAN_POINT ( 'NONE',  ( -100.6814946224345846, -25.25095776846604068, 5.197789127044065260 ) ) ;
#91916=EDGE_CURVE ( 'NONE', #59954, #11920, #87829, .T. ) ;
#91919=EDGE_CURVE ( 'NONE', #59914, #76224, #96274, .T. ) ;
#91920=B_SPLINE_CURVE_WITH_KNOTS ( 'NONE', 3,
 ( #43761, #15678, #19908, #67113, #5189, #29021, #59993, #82313 ),
 .UNSPECIFIED., .F., .F.,
 ( 4, 2, 2, 4 ),
 ( 0.000000000000000000, 0.002001079623178219757, 0.003001619434767328985, 0.004002159246356438646 ),
 .UNSPECIFIED. ) ;
#91921=CARTESIAN_POINT ( 'NONE',  ( -6.535591236171724105, 18.61618873491671877, -1.500000000000002220 ) ) ;
#91922=ORIENTED_EDGE ( 'NONE', *, *, #68747, .F. ) ;
#91923=CARTESIAN_POINT ( 'NONE',  ( -109.3646889549745111, -25.28083575590260068, 4.081544306722298288 ) ) ;
#91927=B_SPLINE_CURVE_WITH_KNOTS ( 'NONE', 3,
 ( #66866, #52129, #13546, #44515 ),
 .UNSPECIFIED., .F., .F.,
 ( 4, 4 ),
 ( 0.000000000000000000, 9.999999999998897304E-05 ),
 .UNSPECIFIED. ) ;
#91929=CARTESIAN_POINT ( 'NONE',  ( -49.62287095715005592, -29.50250243563736774, 8.947779886222146928 ) ) ;
#91930=CARTESIAN_POINT ( 'NONE',  ( -103.6228709571500843, -24.35013146730204525, 9.818937971375111928 ) ) ;
#91931=CARTESIAN_POINT ( 'NONE',  ( -55.54397260187641194, -24.40034930558990922, 0.3402023900116048494 ) ) ;
#91932=CARTESIAN_POINT ( 'NONE',  ( -98.89534031563961491, -25.03144876920082496, 6.173963160515893556 ) ) ;
#91935=FACE_OUTER_BOUND ( 'NONE', #33253, .T. ) ;
#91936=B_SPLINE_CURVE_WITH_KNOTS ( 'NONE', 3,
 ( #70161, #32597, #31593, #63574, #48842, #24978, #40716, #2169 ),
 .UNSPECIFIED., .F., .F.,
 ( 4, 2, 2, 4 ),
 ( -0.001224554619866335221, -0.0002241820295893557757, 0.0007761905606876236697, 0.002776935741241578874 ),
 .UNSPECIFIED. ) ;
#91937=CARTESIAN_POINT ( 'NONE',  ( -107.6317610820995725, -23.73766607897672642, -1.055555164236427590 ) ) ;
#91938=CARTESIAN_POINT ( 'NONE',  ( -11.50144725928494438, 16.33591932373696665, -1.500000000000002220 ) ) ;
#91939=EDGE_CURVE ( 'NONE', #15956, #14129, #22370, .T. ) ;
#91940=CARTESIAN_POINT ( 'NONE',  ( -125.6228709571500559, -24.15516710230296482, 10.28746687063724607 ) ) ;
#91941=CARTESIAN_POINT ( 'NONE',  ( -45.47188313039849561, -25.00182538069146787, 7.747789668545044250 ) ) ;
#91942=EDGE_LOOP ( 'NONE', ( #38318, #19727, #43393, #52525 ) ) ;
#91945=CARTESIAN_POINT ( 'NONE',  ( -80.58514661375853905, -24.73531770709095312, 8.716586749053508498 ) ) ;
#91946=CARTESIAN_POINT ( 'NONE',  ( -58.52287095715006870, -24.51387760970724372, 9.387446482453404073 ) ) ;
#91947=CARTESIAN_POINT ( 'NONE',  ( -81.51736575286189179, -23.73766607897671221, -1.055555164236432919 ) ) ;
#91949=CARTESIAN_POINT ( 'NONE',  ( -51.19681519762799127, -25.31574444707050731, 4.857314373449191258 ) ) ;
#91950=CARTESIAN_POINT ( 'NONE',  ( -118.6228709571500559, -29.50247984919015209, -1.443849546365046699 ) ) ;
#91951=FACE_OUTER_BOUND ( 'NONE', #68912, .T. ) ;
#91952=ORIENTED_EDGE ( 'NONE', *, *, #51179, .F. ) ;
#91953=CARTESIAN_POINT ( 'NONE',  ( -19.72078065558051208, -4.686549088087978099, -1.500000000000002220 ) ) ;
#91954=CARTESIAN_POINT ( 'NONE',  ( -77.52287095715006160, -23.47596703998600631, 11.44779298504228571 ) ) ;
#91955=LINE ( 'NONE', #13826, #1544 ) ;
#91957=PLANE ( 'NONE',  #26562 ) ;
#91959=ORIENTED_EDGE ( 'NONE', *, *, #4195, .T. ) ;
#91962=CARTESIAN_POINT ( 'NONE',  ( 15.80722972286721983, -12.41807379269815215, -1.500000000000002220 ) ) ;
#91963=CARTESIAN_POINT ( 'NONE',  ( -10.38599875782317206, -18.32754119035049101, 11.49999999999999645 ) ) ;
#91965=CARTESIAN_POINT ( 'NONE',  ( -99.55620429048337883, -24.64965694238574656, 8.947790433994192938 ) ) ;
#91966=CARTESIAN_POINT ( 'NONE',  ( -19.76278938440450617, -9.944092408650034187, -1.500000000000002220 ) ) ;
#91968=CARTESIAN_POINT ( 'NONE',  ( -6.383830130275963910, 19.51498944528526991, -1.500000000000002220 ) ) ;
#91969=CARTESIAN_POINT ( 'NONE',  ( -39.44984910185593208, -25.31589155146792791, 4.278338758482362891 ) ) ;
#91970=CARTESIAN_POINT ( 'NONE',  ( -60.58907311184719902, -24.52300882791528380, 0.6510814631126233820 ) ) ;
#91973=EDGE_LOOP ( 'NONE', ( #35642, #91220, #17880, #17966 ) ) ;
#91974=CARTESIAN_POINT ( 'NONE',  ( -35.52287095715006870, -24.52323809116984421, 9.355190652339436141 ) ) ;
#91975=PLANE ( 'NONE',  #33988 ) ;
#91980=CARTESIAN_POINT ( 'NONE',  ( -71.62287095715009855, -24.33927499327855060, 9.819080762295815390 ) ) ;
#91981=CARTESIAN_POINT ( 'NONE',  ( -77.52287095715006160, -24.65952944569304606, 1.056160979905698794 ) ) ;
#91982=CARTESIAN_POINT ( 'NONE',  ( 20.52162115075873672, 2.272738508513782119, -1.500000000000002220 ) ) ;
#91983=CARTESIAN_POINT ( 'NONE',  ( -5.517532219241116032, 20.92096086382833064, 11.49999999999999645 ) ) ;
#91985=DIRECTION ( 'NONE',  ( 0.000000000000000000, -2.173523156925979552E-06, 0.9999999999976378895 ) ) ;
#91987=CARTESIAN_POINT ( 'NONE',  ( -21.65924713590726469, 5.634197536097032888, 11.49999999999998934 ) ) ;
#91988=CARTESIAN_POINT ( 'NONE',  ( -80.37464638460068045, -25.27875090142109826, 7.098502068079202587 ) ) ;
#91989=CARTESIAN_POINT ( 'NONE',  ( -84.59179061558366186, -24.15543982623907482, -0.2315651400026629836 ) ) ;
#91992=CARTESIAN_POINT ( 'NONE',  ( -49.62369280273893679, -24.66019654487198665, 8.947790411086131712 ) ) ;
#91993=CARTESIAN_POINT ( 'NONE',  ( -20.67734376658059858, -3.193854526364364954, 11.49999999999998934 ) ) ;
#91995=CARTESIAN_POINT ( 'NONE',  ( -86.56264050182306846, -23.48783264082478084, -1.443836473390066377 ) ) ;
#91998=ORIENTED_EDGE ( 'NONE', *, *, #11289, .T. ) ;
#91999=CARTESIAN_POINT ( 'NONE',  ( -109.5201641829940797, -23.73791477778912551, 11.05961554403169878 ) ) ;
#92000=CARTESIAN_POINT ( 'NONE',  ( 4.708956132399880978, 20.65895737721473679, -1.500000000000002220 ) ) ;
#92003=CARTESIAN_POINT ( 'NONE',  ( -99.53757426446047418, -25.12215597945658985, 6.745911859225921070 ) ) ;
#92004=CARTESIAN_POINT ( 'NONE',  ( 13.71991279636371175, 16.93377936151356877, -1.500000000000002220 ) ) ;
#92009=CARTESIAN_POINT ( 'NONE',  ( 6.829227106855087825, -20.66181959361685827, -1.500000000000002220 ) ) ;
#92011=CARTESIAN_POINT ( 'NONE',  ( -18.97848940637192428, 11.77069306843248064, 11.49999999999999645 ) ) ;
#92012=VERTEX_POINT ( 'NONE', #44310 ) ;
#92013=CARTESIAN_POINT ( 'NONE',  ( -77.52287095715010423, -23.47593901973090524, -1.443836447538997092 ) ) ;
#92014=CARTESIAN_POINT ( 'NONE',  ( -123.5228709571500616, -24.65952944569304961, 1.056160979905705899 ) ) ;
#92016=EDGE_LOOP ( 'NONE', ( #2153, #20436, #93922, #87535 ) ) ;
#92017=ORIENTED_EDGE ( 'NONE', *, *, #31925, .T. ) ;
#92018=ORIENTED_EDGE ( 'NONE', *, *, #82199, .T. ) ;
#92019=B_SPLINE_CURVE_WITH_KNOTS ( 'NONE', 3,
 ( #28164, #75320, #60624, #16296 ),
 .UNSPECIFIED., .F., .F.,
 ( 4, 4 ),
 ( 0.000000000000000000, 0.0001000000000000028644 ),
 .UNSPECIFIED. ) ;
#92020=CARTESIAN_POINT ( 'NONE',  ( -124.5895376238167529, -24.66019654487200441, 8.947790411086115725 ) ) ;
#92021=CARTESIAN_POINT ( 'NONE',  ( 16.79009078985406234, 12.93418496121567252, 11.49999999999998934 ) ) ;
#92023=CARTESIAN_POINT ( 'NONE',  ( -95.62287095714997065, -24.51254535404256885, 9.355368623467656519 ) ) ;
#92024=LINE ( 'NONE', #91525, #72974 ) ;
#92025=CARTESIAN_POINT ( 'NONE',  ( -30.57287095715006231, -23.47596702059239604, 11.43887032355635647 ) ) ;
#92026=CARTESIAN_POINT ( 'NONE',  ( -19.23900614489824079, 2.250179475969715348, 11.49999999999998934 ) ) ;
#92028=CARTESIAN_POINT ( 'NONE',  ( -70.10894464503664381, -25.31100528015419826, 5.336487379620773019 ) ) ;
#92030=ADVANCED_FACE ( 'NONE', ( #61533 ), #82846, .T. ) ;
#92031=CARTESIAN_POINT ( 'NONE',  ( -2.795030477444873540, 19.22867370847827573, 11.49999999999999645 ) ) ;
#92033=ORIENTED_EDGE ( 'NONE', *, *, #29948, .T. ) ;
#92034=EDGE_CURVE ( 'NONE', #10131, #72641, #45304, .T. ) ;
#92037=ADVANCED_FACE ( 'NONE', ( #69124 ), #76714, .T. ) ;
#92038=CARTESIAN_POINT ( 'NONE',  ( -130.5728709571500872, -23.78087380709146359, 10.97511746239721653 ) ) ;
#92039=CARTESIAN_POINT ( 'NONE',  ( -3.832734262880480358, 19.25313627021017382, 11.49999999999998934 ) ) ;
#92040=B_SPLINE_SURFACE_WITH_KNOTS ( 'NONE', 3, 1, ( 
 ( #63280, #62781 ),
 ( #15572, #100289 ),
 ( #71382, #38417 ),
 ( #93697, #30807 ),
 ( #7964, #94195 ),
 ( #61773, #32305 ),
 ( #47544, #85586 ),
 ( #40426, #63788 ),
 ( #8967, #92691 ),
 ( #23175, #54163 ),
 ( #38918, #69871 ),
 ( #70882, #354 ),
 ( #62269, #1371 ),
 ( #24681, #47043 ),
 ( #77958, #8470 ),
 ( #55665, #11467 ),
 ( #4367, #42933 ),
 ( #18082, #40922 ),
 ( #9969, #34313 ),
 ( #33809, #73376 ),
 ( #11964, #64792 ),
 ( #2368, #35317 ),
 ( #88600, #95708 ),
 ( #58156, #26196 ),
 ( #10973, #72880 ),
 ( #3874, #65290 ),
 ( #72383, #64286 ) ),
 .UNSPECIFIED., .F., .F., .F.,
 ( 4, 1, 1, 1, 1, 1, 1, 1, 1, 1, 1, 1, 1, 1, 1, 1, 1, 1, 1, 1, 1, 1, 1, 1, 4 ),
 ( 2, 2 ),
 ( 0.000000000000000000, 0.06506328961727912696, 0.1267731664665228686, 0.1855157632260792111, 0.2407646791677150733, 0.2929797960235981935, 0.3422503727797673867, 0.3889192861856604622, 0.4327756640583106384, 0.4746284326311178137, 0.5147746906379535581, 0.5536058934984424695, 0.5914264064311730573, 0.6280281199460679975, 0.6638036341103209503, 0.6989843361316647741, 0.7335914893067051468, 0.7676284691511403580, 0.8012083477865920011, 0.8342638397266241013, 0.8669806947287761467, 0.8997197415181606983, 0.9327019124985390652, 0.9661758834327494050, 1.000000000000000000 ),
 ( 0.000000000000000000, 1.000000000000000000 ),
 .UNSPECIFIED. ) ;
#92041=EDGE_CURVE ( 'NONE', #89848, #29762, #7725, .T. ) ;
#92042=CARTESIAN_POINT ( 'NONE',  ( -39.62287095715005592, -24.66019654487199020, 8.947790411086135265 ) ) ;
#92043=ORIENTED_EDGE ( 'NONE', *, *, #50242, .T. ) ;
#92044=CARTESIAN_POINT ( 'NONE',  ( 14.33184905138074683, -16.10332302735202958, 11.49999999999998934 ) ) ;
#92045=CARTESIAN_POINT ( 'NONE',  ( -85.92287095715005307, -23.47596703998600631, 11.44779298504227860 ) ) ;
#92046=ADVANCED_FACE ( 'NONE', ( #60538 ), #67649, .T. ) ;
#92047=DIRECTION ( 'NONE',  ( -3.773278334453079618E-23, 0.9999999999976377785, 2.173523156925979975E-06 ) ) ;
#92049=CARTESIAN_POINT ( 'NONE',  ( -18.14924840124409045, -14.16824886576183040, -1.500000000000002220 ) ) ;
#92051=CARTESIAN_POINT ( 'NONE',  ( -127.2228709571500360, -23.47593901973090524, -1.443836447538996204 ) ) ;
#92052=CARTESIAN_POINT ( 'NONE',  ( -50.70677674236874566, -25.18370859199909972, 3.285367768258824483 ) ) ;
#92053=CARTESIAN_POINT ( 'NONE',  ( -20.14672940031187665, -1.731937678239350298, 11.49999999999999645 ) ) ;
#92054=CARTESIAN_POINT ( 'NONE',  ( -121.5205767367703373, -23.96169478059713853, 10.65365249895717525 ) ) ;
#92056=CARTESIAN_POINT ( 'NONE',  ( -111.6050501299251323, -25.10921541419112302, 3.602892040021733688 ) ) ;
#92058=CARTESIAN_POINT ( 'NONE',  ( -110.5404475696186779, -25.29779158700655728, 3.309296744833758908 ) ) ;
#92059=CARTESIAN_POINT ( 'NONE',  ( 19.57267778704439820, -3.578973306870405047, 11.49999999999998934 ) ) ;
#92061=CARTESIAN_POINT ( 'NONE',  ( -68.92287095715006728, -23.47593901973090169, -1.443836447538997536 ) ) ;
#92062=CARTESIAN_POINT ( 'NONE',  ( -9.637476322613308000, -17.25261889746210997, -1.500000000000002220 ) ) ;
#92063=AXIS2_PLACEMENT_3D ( 'NONE', #95556, #95054, #25035 ) ;
#92064=CARTESIAN_POINT ( 'NONE',  ( -56.52206875506576012, -23.48783264082477018, -1.443836473390095909 ) ) ;
#92065=CARTESIAN_POINT ( 'NONE',  ( -40.07089665442598658, -25.29116527456120522, 2.873457746617287700 ) ) ;
#92066=CARTESIAN_POINT ( 'NONE',  ( -42.52287095715006160, -24.50216790748203977, 0.6166512839542503954 ) ) ;
#92067=CARTESIAN_POINT ( 'NONE',  ( 14.23986175545555355, -14.96101607593195304, 11.49999999999999645 ) ) ;
#92068=CARTESIAN_POINT ( 'NONE',  ( -39.56136241089613037, -25.31628735779903039, 5.536731292741799315 ) ) ;
#92070=FACE_OUTER_BOUND ( 'NONE', #72210, .T. ) ;
#92071=CARTESIAN_POINT ( 'NONE',  ( -13.58842472641693711, -18.21064416987719525, 11.49999999999999645 ) ) ;
#92073=CARTESIAN_POINT ( 'NONE',  ( -67.52287095715006160, -24.64898659630528854, 1.056161002820824368 ) ) ;
#92076=CARTESIAN_POINT ( 'NONE',  ( 17.97931717627152182, 9.192180251422895410, -1.500000000000002220 ) ) ;
#92077=CARTESIAN_POINT ( 'NONE',  ( -108.6228709571500701, -23.72773821059535848, 11.05748984161097503 ) ) ;
#92078=CARTESIAN_POINT ( 'NONE',  ( -45.58953762381672448, -23.48786465467240703, 11.44779295918255002 ) ) ;
#92079=ORIENTED_EDGE ( 'NONE', *, *, #83449, .T. ) ;
#92080=ORIENTED_EDGE ( 'NONE', *, *, #2367, .T. ) ;
#92082=CARTESIAN_POINT ( 'NONE',  ( 18.88093902437788785, 12.95799798663108682, -1.500000000000002220 ) ) ;
#92083=CARTESIAN_POINT ( 'NONE',  ( -41.86183995336322994, -25.27646494108434183, 4.023331222604434210 ) ) ;
#92084=CARTESIAN_POINT ( 'NONE',  ( 21.56569437331729233, -1.927008741106717604, -1.500000000000002220 ) ) ;
#92086=DIRECTION ( 'NONE',  ( 1.000000000000000000, 3.773278334444167608E-23, 8.201307833595939069E-29 ) ) ;
#92087=CARTESIAN_POINT ( 'NONE',  ( -34.65813035707638079, -23.73766607897670866, -1.055555164236443133 ) ) ;
#92088=CARTESIAN_POINT ( 'NONE',  ( -16.12721948686093754, -13.32240427740599564, 11.49999999999999645 ) ) ;
#92089=VERTEX_POINT ( 'NONE', #29064 ) ;
#92090=B_SPLINE_CURVE_WITH_KNOTS ( 'NONE', 3,
 ( #36788, #36294, #20546, #81962 ),
 .UNSPECIFIED., .F., .F.,
 ( 4, 4 ),
 ( 0.000000000000000000, 9.999999999998897304E-05 ),
 .UNSPECIFIED. ) ;
#92091=CARTESIAN_POINT ( 'NONE',  ( -104.5228709571501184, -23.48783264082477373, -1.443836473390087027 ) ) ;
#92092=CARTESIAN_POINT ( 'NONE',  ( 7.855769811932122870, -20.56199346058834720, -1.500000000000002220 ) ) ;
#92093=EDGE_CURVE ( 'NONE', #32532, #46308, #79360, .T. ) ;
#92094=CARTESIAN_POINT ( 'NONE',  ( -105.6261421520168540, -24.73531770709095312, 8.716586749053508498 ) ) ;
#92095=CARTESIAN_POINT ( 'NONE',  ( -41.68940843163829868, -25.10925916055124318, 3.512445505603538187 ) ) ;
#92099=CARTESIAN_POINT ( 'NONE',  ( -90.58606251549953470, -24.73531770709095312, 8.716586749053512051 ) ) ;
#92102=ORIENTED_EDGE ( 'NONE', *, *, #99098, .T. ) ;
#92104=CARTESIAN_POINT ( 'NONE',  ( -71.52210967603697611, -23.48786465467241058, 11.44779295918254824 ) ) ;
#92105=CARTESIAN_POINT ( 'NONE',  ( -101.7776484685884242, -25.27404881181734808, 3.986250615313824408 ) ) ;
#92106=CARTESIAN_POINT ( 'NONE',  ( -100.5228709571500758, -24.51254535375843702, 9.355368624242247577 ) ) ;
#92107=CARTESIAN_POINT ( 'NONE',  ( 20.06376955418885899, 4.186446014007643157, -1.500000000000002220 ) ) ;
#92108=ORIENTED_EDGE ( 'NONE', *, *, #65642, .F. ) ;
#92110=DIRECTION ( 'NONE',  ( -3.773278334453080206E-23, 0.9999999999976377785, 2.173523156925979975E-06 ) ) ;
#92111=CARTESIAN_POINT ( 'NONE',  ( -99.58953762381672448, -23.48783264082478794, -1.443836473390061936 ) ) ;
#92112=CARTESIAN_POINT ( 'NONE',  ( -18.06118310651259407, 13.05043149098080058, -1.500000000000002220 ) ) ;
#92113=CARTESIAN_POINT ( 'NONE',  ( -74.62287095715005592, -29.50250243563736774, 8.947779886222143375 ) ) ;
#92117=CARTESIAN_POINT ( 'NONE',  ( -29.60812400815161283, -24.63645724241111168, 6.685405290659707234 ) ) ;
#92118=CARTESIAN_POINT ( 'NONE',  ( 16.81283763619640936, 12.23492182941471107, 11.49999999999998934 ) ) ;
#92119=EDGE_LOOP ( 'NONE', ( #14012, #27252, #13243, #17631 ) ) ;
#92120=EDGE_CURVE ( 'NONE', #61188, #10228, #84343, .T. ) ;
#92121=CARTESIAN_POINT ( 'NONE',  ( -54.62287095715004881, -24.50216790748096685, 0.6166512839513625943 ) ) ;
#92123=B_SPLINE_SURFACE_WITH_KNOTS ( 'NONE', 3, 3, ( 
 ( #37565, #60916, #84732, #46689 ),
 ( #13715, #15223, #70012, #498 ),
 ( #60421, #46181, #44687, #91346 ),
 ( #21821, #91843, #77109, #22319 ),
 ( #69520, #55308, #86240, #63938 ),
 ( #54803, #16224, #40577, #10620 ),
 ( #86737, #47189, #56815, #17226 ) ),
 .UNSPECIFIED., .F., .F., .F.,
 ( 4, 3, 4 ),
 ( 4, 4 ),
 ( 0.7945040050992233649, 0.8970133687736494554, 0.9995227324480754350 ),
 ( 0.2195497878891723154, 0.2206638711953707588 ),
 .UNSPECIFIED. ) ;
#92124=CARTESIAN_POINT ( 'NONE',  ( -98.52287095715006160, -23.48786465467241769, 11.44779295918254114 ) ) ;
#92128=CARTESIAN_POINT ( 'NONE',  ( -50.72667573002448904, -25.10935765147311471, 2.869183402993591425 ) ) ;
#92130=CARTESIAN_POINT ( 'NONE',  ( -60.62287095715004881, -29.50250786944525672, 11.44777988621623876 ) ) ;
#92131=CARTESIAN_POINT ( 'NONE',  ( -109.2249784094242244, -25.20198318546772498, 3.338762932793643223 ) ) ;
#92132=CARTESIAN_POINT ( 'NONE',  ( -43.62287095715004881, -29.50250243563736774, 8.947779886222148704 ) ) ;
#92133=CARTESIAN_POINT ( 'NONE',  ( 21.55033589006239936, 5.121329677682045833, 11.49999999999999645 ) ) ;
#92135=CARTESIAN_POINT ( 'NONE',  ( -44.62287095715005592, -24.51387760970723662, 9.387446482453432495 ) ) ;
#92136=CARTESIAN_POINT ( 'NONE',  ( -22.51868310087907687, -2.221351303042197411, 11.49999999999998934 ) ) ;
#92138=CARTESIAN_POINT ( 'NONE',  ( -28.74698468279304819, -24.98503885035050942, 7.079829357813114399 ) ) ;
#92142=CARTESIAN_POINT ( 'NONE',  ( 10.61947033613929214, 17.11087026910869469, -1.500000000000002220 ) ) ;
#92143=CARTESIAN_POINT ( 'NONE',  ( -71.52287095715007581, -29.50248528299804818, 1.056150453629036701 ) ) ;
#92144=ORIENTED_EDGE ( 'NONE', *, *, #5153, .F. ) ;
#92145=VECTOR ( 'NONE', #99311, 1000.000000000000114 ) ;
#92146=CARTESIAN_POINT ( 'NONE',  ( -39.62287095715005592, -23.48786465467240347, 11.44779295918255180 ) ) ;
#92147=CARTESIAN_POINT ( 'NONE',  ( -22.28969446433750434, -1.297463027894488086, -1.500000000000002220 ) ) ;
#92148=ORIENTED_EDGE ( 'NONE', *, *, #1444, .F. ) ;
#92149=VERTEX_POINT ( 'NONE', #45795 ) ;
#92151=CARTESIAN_POINT ( 'NONE',  ( -34.62287095715005592, -29.50248528299804818, 1.056150453629029817 ) ) ;
#92152=ADVANCED_FACE ( 'NONE', ( #7216 ), #30562, .T. ) ;
#92153=FACE_OUTER_BOUND ( 'NONE', #57773, .T. ) ;
#92155=LINE ( 'NONE', #84546, #65058 ) ;
#92156=CARTESIAN_POINT ( 'NONE',  ( 17.64699390344983598, -8.409456921668478913, -1.500000000000002220 ) ) ;
#92157=EDGE_CURVE ( 'NONE', #10237, #68291, #23643, .T. ) ;
#92158=CARTESIAN_POINT ( 'NONE',  ( -102.5228709571501327, -23.73907113217669007, -1.053371485781297023 ) ) ;
#92159=CARTESIAN_POINT ( 'NONE',  ( -21.25412285906045895, 3.082840150875858054, -1.500000000000002220 ) ) ;
#92160=CARTESIAN_POINT ( 'NONE',  ( -25.53440485667337612, -24.58000155304849699, 4.657483218939315606 ) ) ;
#92162=B_SPLINE_CURVE_WITH_KNOTS ( 'NONE', 3,
 ( #24597, #86504, #47956, #40337, #71289, #80896 ),
 .UNSPECIFIED., .F., .F.,
 ( 4, 2, 4 ),
 ( 1.570755371633777598E-05, 0.001396183895866084934, 0.002776660238015832109 ),
 .UNSPECIFIED. ) ;
#92165=CARTESIAN_POINT ( 'NONE',  ( 10.78062712001149492, -20.16176685268226976, -1.500000000000002220 ) ) ;
#92166=B_SPLINE_CURVE_WITH_KNOTS ( 'NONE', 3,
 ( #93773, #39992, #54233, #62341 ),
 .UNSPECIFIED., .F., .F.,
 ( 4, 4 ),
 ( 0.2099358345183179875, 0.2189422657904334657 ),
 .UNSPECIFIED. ) ;
#92167=VECTOR ( 'NONE', #83051, 1000.000000000000114 ) ;
#92169=DIRECTION ( 'NONE',  ( 0.000000000000000000, -0.9999999999976377785, -2.173523156925979975E-06 ) ) ;
#92171=CARTESIAN_POINT ( 'NONE',  ( -7.473237707827510512, 18.53023608995856009, 11.49999999999999645 ) ) ;
#92172=CARTESIAN_POINT ( 'NONE',  ( -89.40841769935767047, -25.06732983082694943, 7.447789526168953955 ) ) ;
#92174=CARTESIAN_POINT ( 'NONE',  ( -108.6228709571500275, -23.72747288104442021, -1.053458166803660889 ) ) ;
#92176=EDGE_CURVE ( 'NONE', #18738, #8368, #59973, .T. ) ;
#92178=CARTESIAN_POINT ( 'NONE',  ( -114.5562042904833788, -24.64898659630529210, 1.056161002820829475 ) ) ;
#92179=CARTESIAN_POINT ( 'NONE',  ( -12.78816955685674372, 17.57309652720472570, -1.500000000000002220 ) ) ;
#92180=CARTESIAN_POINT ( 'NONE',  ( -108.6228709571500559, -24.64965695001468404, 8.947790433994176951 ) ) ;
#92181=CARTESIAN_POINT ( 'NONE',  ( 16.12930680145378304, -11.13525102954884893, -1.500000000000002220 ) ) ;
#92182=DIRECTION ( 'NONE',  ( -3.773278334453080206E-23, 0.9999999999976377785, 2.173523156925979975E-06 ) ) ;
#92183=CARTESIAN_POINT ( 'NONE',  ( -41.43233941641154416, -25.25932830633372461, 3.941234411137095606 ) ) ;
#92186=CARTESIAN_POINT ( 'NONE',  ( -124.2228709571500502, -23.47596703998600631, 11.44779298504227860 ) ) ;
#92187=CARTESIAN_POINT ( 'NONE',  ( -17.34406541665444124, 10.97931167347951842, 11.49999999999999645 ) ) ;
#92192=DIRECTION ( 'NONE',  ( -3.773278334453079030E-23, 0.9999999999976377785, 2.173523156925979128E-06 ) ) ;
#92193=CARTESIAN_POINT ( 'NONE',  ( -39.67258447180102365, -25.18430942437969122, 3.621101466496972066 ) ) ;
#92194=VECTOR ( 'NONE', #100174, 1000.000000000000114 ) ;
#92195=CARTESIAN_POINT ( 'NONE',  ( -125.5916857295030553, -23.48786465467241413, 11.44779295918253581 ) ) ;
#92196=CARTESIAN_POINT ( 'NONE',  ( -85.62287095715004170, -23.48783264082478794, -1.443836473390063713 ) ) ;
#92200=B_SPLINE_CURVE_WITH_KNOTS ( 'NONE', 3,
 ( #19057, #95190, #25674, #49030, #82455, #4351 ),
 .UNSPECIFIED., .F., .F.,
 ( 4, 2, 4 ),
 ( 0.000000000000000000, 0.001380901958385387027, 0.002761803916770774053 ),
 .UNSPECIFIED. ) ;
#92202=CARTESIAN_POINT ( 'NONE',  ( -22.67921066581790868, 4.291001918001082771, 11.49999999999999645 ) ) ;
#92203=CARTESIAN_POINT ( 'NONE',  ( -15.22011711465338912, -17.00649957279452451, -1.500000000000002220 ) ) ;
#92204=CARTESIAN_POINT ( 'NONE',  ( -74.52211797261165316, -23.48783264082477018, -1.443836473390096353 ) ) ;
#92206=CARTESIAN_POINT ( 'NONE',  ( -60.45647493444359810, -25.28662977279051560, 6.028426056058751037 ) ) ;
#92207=B_SPLINE_CURVE_WITH_KNOTS ( 'NONE', 3,
 ( #5556, #80687, #12666, #42150 ),
 .UNSPECIFIED., .F., .F.,
 ( 4, 4 ),
 ( 0.000000000000000000, 1.000000000000000000 ),
 .UNSPECIFIED. ) ;
#92208=CARTESIAN_POINT ( 'NONE',  ( 6.649717926671450563, 21.43536518531312396, 11.49999999999999645 ) ) ;
#92211=CARTESIAN_POINT ( 'NONE',  ( -38.62287095715007013, -23.95044443724992078, 10.65354141964649592 ) ) ;
#92212=CARTESIAN_POINT ( 'NONE',  ( -17.33335002049248530, 13.43749923854009509, -1.500000000000002220 ) ) ;
#92215=CARTESIAN_POINT ( 'NONE',  ( -87.62602049761908063, -24.51419770103156281, 9.386484678747175181 ) ) ;
#92216=CARTESIAN_POINT ( 'NONE',  ( -33.52287095715006160, -23.48786465467240347, 11.44779295918255357 ) ) ;
#92217=CARTESIAN_POINT ( 'NONE',  ( -78.49839763410953708, -24.65952944569304606, 1.056160979905704789 ) ) ;
#92220=VECTOR ( 'NONE', #44800, 1000.000000000000114 ) ;
#92221=CARTESIAN_POINT ( 'NONE',  ( 20.41236503877875563, 1.188189311754236144, 11.49999999999998934 ) ) ;
#92226=CARTESIAN_POINT ( 'NONE',  ( -22.67921066581790868, 4.291001918001082771, 11.49999999999998934 ) ) ;
#92227=CARTESIAN_POINT ( 'NONE',  ( -39.43812566566255384, -25.18341647909762315, 3.283321612209681994 ) ) ;
#92228=CARTESIAN_POINT ( 'NONE',  ( -17.45352675615719917, 10.31968153043333380, -1.500000000000002220 ) ) ;
#92230=CARTESIAN_POINT ( 'NONE',  ( -122.5228709571501042, -24.33832256527049154, 0.1851278514138668951 ) ) ;
#92231=CARTESIAN_POINT ( 'NONE',  ( -41.69070460756492480, -25.31528773746466143, 4.890768902268528784 ) ) ;
#92232=CARTESIAN_POINT ( 'NONE',  ( -94.52287095715006160, -23.47596703998600631, 11.44779298504228393 ) ) ;
#92233=CARTESIAN_POINT ( 'NONE',  ( -70.55922828164491989, -23.85016227208580730, -0.8807180028928335291 ) ) ;
#92234=CARTESIAN_POINT ( 'NONE',  ( -3.867184171070207288, -21.11305558764578194, 11.49999999999999645 ) ) ;
#92235=ORIENTED_EDGE ( 'NONE', *, *, #74955, .T. ) ;
#92238=ORIENTED_EDGE ( 'NONE', *, *, #16444, .F. ) ;
#92239=CARTESIAN_POINT ( 'NONE',  ( 20.67342648114324533, -1.018679444107209342, -1.500000000000002220 ) ) ;
#92244=ORIENTED_EDGE ( 'NONE', *, *, #97201, .T. ) ;
#92245=B_SPLINE_CURVE_WITH_KNOTS ( 'NONE', 3,
 ( #20752, #50727, #81672, #28373 ),
 .UNSPECIFIED., .F., .F.,
 ( 4, 4 ),
 ( 0.000000000000000000, 9.999999999998897304E-05 ),
 .UNSPECIFIED. ) ;
#92246=CARTESIAN_POINT ( 'NONE',  ( -28.52198438452846574, -23.32368101661869275, -1.443835813551990865 ) ) ;
#92250=CARTESIAN_POINT ( 'NONE',  ( -65.53231158233933229, -24.92564183028979130, 1.928384488918254869 ) ) ;
#92251=CARTESIAN_POINT ( 'NONE',  ( 20.73430856240977249, 7.200853762728330665, 11.49999999999999645 ) ) ;
#92253=CARTESIAN_POINT ( 'NONE',  ( 1.525329354412473970, -22.51392980886878448, 11.49999999999998934 ) ) ;
#92254=ADVANCED_FACE ( 'NONE', ( #39673 ), #16334, .F. ) ;
#92255=CARTESIAN_POINT ( 'NONE',  ( -20.02981537788295441, -6.213780249082809348, -1.500000000000002220 ) ) ;
#92256=CARTESIAN_POINT ( 'NONE',  ( -124.6228709571500559, -29.50248528299804818, 1.056150453629045360 ) ) ;
#92258=ORIENTED_EDGE ( 'NONE', *, *, #56853, .T. ) ;
#92259=ORIENTED_EDGE ( 'NONE', *, *, #100027, .F. ) ;
#92262=CARTESIAN_POINT ( 'NONE',  ( -14.35963886870962192, 16.04489112172382903, -1.500000000000002220 ) ) ;
#92265=CARTESIAN_POINT ( 'NONE',  ( -15.95541298346445735, 13.85296639876547076, 11.49999999999998934 ) ) ;
#92267=CARTESIAN_POINT ( 'NONE',  ( -89.81226385320383088, -29.50249166729307149, 3.993452963156916002 ) ) ;
#92269=CARTESIAN_POINT ( 'NONE',  ( -50.17717618564654458, -25.30219648044955250, 4.715273004579882077 ) ) ;
#92270=FACE_OUTER_BOUND ( 'NONE', #9697, .T. ) ;
#92272=CARTESIAN_POINT ( 'NONE',  ( 20.51613352552997327, 8.347415244503286758, -1.500000000000002220 ) ) ;
#92273=CARTESIAN_POINT ( 'NONE',  ( -112.5228709571500616, -23.48783264083431988, -1.443836473375253782 ) ) ;
#92274=EDGE_CURVE ( 'NONE', #47959, #17515, #23946, .T. ) ;
#92275=ORIENTED_EDGE ( 'NONE', *, *, #59167, .T. ) ;
#92276=CARTESIAN_POINT ( 'NONE',  ( -51.66594184980125704, -25.31633186406339675, 5.409172801058263147 ) ) ;
#92280=CARTESIAN_POINT ( 'NONE',  ( -100.5441727580858782, -25.00158670708910691, 2.256160236439218369 ) ) ;
#92281=AXIS2_PLACEMENT_3D ( 'NONE', #14823, #76711, #14322 ) ;
#92282=CARTESIAN_POINT ( 'NONE',  ( 19.43689267596983683, 0.5339526363925560792, -1.500000000000002220 ) ) ;
#92285=B_SPLINE_CURVE_WITH_KNOTS ( 'NONE', 3,
 ( #93975, #23961, #64567, #630 ),
 .UNSPECIFIED., .F., .F.,
 ( 4, 4 ),
 ( 0.000000000000000000, 9.999999999998897304E-05 ),
 .UNSPECIFIED. ) ;
#92286=CARTESIAN_POINT ( 'NONE',  ( 6.831138157384286203, 20.27010762675863731, 11.49999999999998934 ) ) ;
#92287=CARTESIAN_POINT ( 'NONE',  ( -38.52287095715007581, -24.35013146730203815, 9.818937971375103047 ) ) ;
#92292=CARTESIAN_POINT ( 'NONE',  ( -19.66899025692886838, 11.29834648773183581, -1.500000000000002220 ) ) ;
#92294=CARTESIAN_POINT ( 'NONE',  ( -106.6228709571500559, -23.47593901973091235, -1.443836447538999312 ) ) ;
#92295=FACE_OUTER_BOUND ( 'NONE', #40984, .T. ) ;
#92296=CARTESIAN_POINT ( 'NONE',  ( -11.78406182805296254, 15.88391379356440503, 11.49999999999999645 ) ) ;
#92298=ORIENTED_EDGE ( 'NONE', *, *, #12415, .T. ) ;
#92299=EDGE_CURVE ( 'NONE', #45608, #833, #98573, .T. ) ;
#92300=CARTESIAN_POINT ( 'NONE',  ( -66.62287095715005592, -24.64898659630367916, 1.056161002820824368 ) ) ;
#92301=PLANE ( 'NONE',  #1009 ) ;
#92302=CARTESIAN_POINT ( 'NONE',  ( 16.53012286974688294, -13.99140274789385252, -1.500000000000002220 ) ) ;
#92303=CARTESIAN_POINT ( 'NONE',  ( -29.62287095715005592, -24.42708174548585731, 9.387659993670769865 ) ) ;
#92304=CARTESIAN_POINT ( 'NONE',  ( -17.77321681866180469, -7.816401696202086136, -1.500000000000002220 ) ) ;
#92305=CARTESIAN_POINT ( 'NONE',  ( -82.52287095715006160, -23.48786465467241058, 11.44779295918254469 ) ) ;
#92306=CARTESIAN_POINT ( 'NONE',  ( -35.62287095715004881, -23.48783264082477729, -1.443836473390072372 ) ) ;
#92307=CARTESIAN_POINT ( 'NONE',  ( -4.880483578727112359, 19.22116399702514045, -1.500000000000002220 ) ) ;
#92308=B_SPLINE_CURVE_WITH_KNOTS ( 'NONE', 3,
 ( #88170, #64355, #26764, #72948 ),
 .UNSPECIFIED., .F., .F.,
 ( 4, 4 ),
 ( 0.000000000000000000, 9.999999999999592548E-05 ),
 .UNSPECIFIED. ) ;
#92309=ORIENTED_EDGE ( 'NONE', *, *, #22888, .T. ) ;
#92310=CARTESIAN_POINT ( 'NONE',  ( 13.61570878652767291, 15.11107311891478666, 11.49999999999999645 ) ) ;
#92311=CARTESIAN_POINT ( 'NONE',  ( -80.58925929066886340, -24.52300882791530157, 0.6510814631126378149 ) ) ;
#92312=CARTESIAN_POINT ( 'NONE',  ( -123.6228709571500559, -29.50248528299804818, 1.056150453629045360 ) ) ;
#92313=EDGE_LOOP ( 'NONE', ( #93462, #24940, #30116, #37158 ) ) ;
#92314=B_SPLINE_SURFACE_WITH_KNOTS ( 'NONE', 3, 3, ( 
 ( #64545, #48294, #25445, #32055 ),
 ( #63028, #56421, #24439, #26459 ),
 ( #48804, #57423, #79727, #95456 ),
 ( #55410, #41181, #86349, #72138 ),
 ( #2625, #87852, #80235, #88352 ),
 ( #16831, #10729, #41693, #34071 ),
 ( #97939, #74126, #59910, #36550 ) ),
 .UNSPECIFIED., .F., .F., .F.,
 ( 4, 3, 4 ),
 ( 4, 4 ),
 ( 0.3389043340504380719, 0.5146335846998003616, 0.6903628353491626513 ),
 ( 0.2860456367239210818, 0.3169887994066197812 ),
 .UNSPECIFIED. ) ;
#92315=CARTESIAN_POINT ( 'NONE',  ( -105.5228709571500758, -29.50248528299804818, 1.056150453629043584 ) ) ;
#92317=CARTESIAN_POINT ( 'NONE',  ( -49.03252113942349411, -25.31601947462323920, 5.540384453209895810 ) ) ;
#92318=CARTESIAN_POINT ( 'NONE',  ( -40.49851917831725245, -24.15602025860895097, 10.28564288303536856 ) ) ;
#92319=CARTESIAN_POINT ( 'NONE',  ( -128.6228709571500417, -29.50250243563736774, 8.947779886222132717 ) ) ;
#92320=CARTESIAN_POINT ( 'NONE',  ( -17.52916707085001136, 9.785066945116392745, -1.500000000000002220 ) ) ;
#92322=EDGE_LOOP ( 'NONE', ( #57232, #64845, #1079, #9780 ) ) ;
#92323=CARTESIAN_POINT ( 'NONE',  ( -91.62287095715004170, -24.66019654487199730, 8.947790411086124607 ) ) ;
#92324=CARTESIAN_POINT ( 'NONE',  ( -19.55383134093860420, 11.88776249338449986, 11.49999999999999645 ) ) ;
#92325=CARTESIAN_POINT ( 'NONE',  ( -17.66434017299383896, 14.31182286555179139, -1.500000000000002220 ) ) ;
#92326=CARTESIAN_POINT ( 'NONE',  ( -50.16163650206989644, -25.26258880167387488, 4.712129156570222577 ) ) ;
#92327=DIRECTION ( 'NONE',  ( -3.773278334453079618E-23, 0.9999999999976377785, 2.173523156925979975E-06 ) ) ;
#92328=CARTESIAN_POINT ( 'NONE',  ( -31.24388727629347784, -24.87219037989215309, 1.747789950310770779 ) ) ;
#92332=ADVANCED_FACE ( 'NONE', ( #15830 ), #70128, .T. ) ;
#92333=CARTESIAN_POINT ( 'NONE',  ( -101.5228709571500758, -29.50250243563736774, 8.947779886222138046 ) ) ;
#92335=AXIS2_PLACEMENT_3D ( 'NONE', #37695, #53933, #21950 ) ;
#92336=CARTESIAN_POINT ( 'NONE',  ( 14.56535739210195857, -14.21638276092092745, -1.500000000000002220 ) ) ;
#92337=ORIENTED_EDGE ( 'NONE', *, *, #86902, .F. ) ;
#92338=CARTESIAN_POINT ( 'NONE',  ( -7.281717392095591102, 21.80608952751712692, -1.500000000000002220 ) ) ;
#92339=FACE_OUTER_BOUND ( 'NONE', #51070, .T. ) ;
#92342=FACE_OUTER_BOUND ( 'NONE', #12518, .T. ) ;
#92344=VECTOR ( 'NONE', #18358, 1000.000000000000114 ) ;
#92345=CARTESIAN_POINT ( 'NONE',  ( -40.62287095715004881, -24.14321612903114556, -0.2833117244521690670 ) ) ;
#92346=CARTESIAN_POINT ( 'NONE',  ( 0.1273799443098547757, 21.28700333820561497, 11.49999999999999645 ) ) ;
#92347=VERTEX_POINT ( 'NONE', #70629 ) ;
#92349=ORIENTED_EDGE ( 'NONE', *, *, #42932, .T. ) ;
#92350=CARTESIAN_POINT ( 'NONE',  ( 12.10043277420606778, 18.60588626676543100, 11.49999999999998934 ) ) ;
#92351=CARTESIAN_POINT ( 'NONE',  ( 1.647368763193059582, 20.57021071130147405, 11.49999999999998934 ) ) ;
#92352=EDGE_CURVE ( 'NONE', #38564, #46308, #7831, .T. ) ;
#92354=EDGE_LOOP ( 'NONE', ( #4905, #49237, #5157, #64787 ) ) ;
#92355=VERTEX_POINT ( 'NONE', #1125 ) ;
#92356=CARTESIAN_POINT ( 'NONE',  ( -109.1951039547969202, -25.31627293009379187, 4.973673916210892720 ) ) ;
#92357=CARTESIAN_POINT ( 'NONE',  ( -56.62287095715006302, -24.51283580621364777, 0.6167428607019728171 ) ) ;
#92358=ORIENTED_EDGE ( 'NONE', *, *, #69473, .T. ) ;
#92360=ADVANCED_FACE ( 'NONE', ( #16839 ), #84199, .T. ) ;
#92362=CARTESIAN_POINT ( 'NONE',  ( -126.1692044365139225, -25.21250203164489889, 3.500954016957966264 ) ) ;
#92363=CARTESIAN_POINT ( 'NONE',  ( -44.52287095715006160, -24.50216790748204332, 0.6166512839542455104 ) ) ;
#92364=CARTESIAN_POINT ( 'NONE',  ( 18.03836333725549324, -10.36167025447706713, -1.500000000000002220 ) ) ;
#92365=CARTESIAN_POINT ( 'NONE',  ( -19.96617879207914825, 8.700599545123990808, 11.49999999999999645 ) ) ;
#92368=CARTESIAN_POINT ( 'NONE',  ( -19.72384299526936857, -10.77339039931002773, 11.49999999999998934 ) ) ;
#92372=ORIENTED_EDGE ( 'NONE', *, *, #65642, .T. ) ;
#92375=EDGE_CURVE ( 'NONE', #34336, #15522, #52592, .T. ) ;
#92376=ORIENTED_EDGE ( 'NONE', *, *, #75381, .F. ) ;
#92377=VERTEX_POINT ( 'NONE', #97467 ) ;
#92379=CARTESIAN_POINT ( 'NONE',  ( 0.2649960030224881025, 21.33594185153759426, -1.500000000000002220 ) ) ;
#92381=CARTESIAN_POINT ( 'NONE',  ( 16.43158684610488862, 13.14696595092960152, 11.49999999999998934 ) ) ;
#92382=CARTESIAN_POINT ( 'NONE',  ( -30.57655055308772418, -25.31557562294173280, 3.857144010898052588 ) ) ;
#92383=CARTESIAN_POINT ( 'NONE',  ( -100.0133086385735908, -25.19440624866216893, 3.361853740790277989 ) ) ;
#92385=CARTESIAN_POINT ( 'NONE',  ( 21.30657626330824783, 5.479626006175059239, -1.500000000000002220 ) ) ;
#92386=CARTESIAN_POINT ( 'NONE',  ( -39.52287095715004739, -23.73907113216988307, -1.053371485793256124 ) ) ;
#92387=ORIENTED_EDGE ( 'NONE', *, *, #37526, .F. ) ;
#92389=EDGE_CURVE ( 'NONE', #32935, #15956, #39278, .T. ) ;
#92390=CARTESIAN_POINT ( 'NONE',  ( -55.52287095715008292, -23.47593901973090169, -1.443836447538997092 ) ) ;
#92391=CARTESIAN_POINT ( 'NONE',  ( -84.64007757551536315, -23.73791477778912196, 11.05961554403170588 ) ) ;
#92392=CARTESIAN_POINT ( 'NONE',  ( -106.5228709571500758, -29.50250243563736774, 8.947779886222136270 ) ) ;
#92393=CARTESIAN_POINT ( 'NONE',  ( -10.20960514438541011, -23.56704696218565687, 7.291654623549827186 ) ) ;
#92394=CARTESIAN_POINT ( 'NONE',  ( 6.245503531335690361, -20.37428601906679759, -1.500000000000002220 ) ) ;
#92395=CARTESIAN_POINT ( 'NONE',  ( -46.52287095715006160, -23.48786465467241058, 11.44779295918255002 ) ) ;
#92396=CARTESIAN_POINT ( 'NONE',  ( -107.5162098792497858, -24.15620529776628800, 10.23563542870659759 ) ) ;
#92397=AXIS2_PLACEMENT_3D ( 'NONE', #11251, #57946, #44207 ) ;
#92398=EDGE_CURVE ( 'NONE', #20987, #70270, #58913, .T. ) ;
#92399=CARTESIAN_POINT ( 'NONE',  ( -70.52287095715007581, -24.99132157543166599, 2.256160258750667502 ) ) ;
#92400=CARTESIAN_POINT ( 'NONE',  ( 3.433349652534986696, 22.22849440524942111, -1.500000000000002220 ) ) ;
#92402=CARTESIAN_POINT ( 'NONE',  ( -111.9715540114818566, -25.25626643526282322, 3.571638612575482874 ) ) ;
#92403=ORIENTED_EDGE ( 'NONE', *, *, #55709, .T. ) ;
#92404=CARTESIAN_POINT ( 'NONE',  ( -119.5562042904834072, -24.65952944569305316, 1.056160979905705677 ) ) ;
#92405=CARTESIAN_POINT ( 'NONE',  ( 19.58216393897113505, 1.562425146961006650, 11.49999999999999645 ) ) ;
#92407=CARTESIAN_POINT ( 'NONE',  ( -100.6228709571500701, -24.62285846362215835, 9.038163152653526211 ) ) ;
#92409=ADVANCED_FACE ( 'NONE', ( #99940 ), #99567, .T. ) ;
#92410=CARTESIAN_POINT ( 'NONE',  ( -88.50802900976825072, -24.35071581493543746, 9.817618358456025263 ) ) ;
#92411=CARTESIAN_POINT ( 'NONE',  ( -36.52287095715006160, -24.50321055353803601, 9.387540953477518713 ) ) ;
#92412=CARTESIAN_POINT ( 'NONE',  ( -89.90102583468038233, -25.31476272485208057, 5.144091107239471938 ) ) ;
#92414=CARTESIAN_POINT ( 'NONE',  ( -5.084378373094740944, 19.06436389234985285, -1.500000000000002220 ) ) ;
#92417=ORIENTED_EDGE ( 'NONE', *, *, #74081, .F. ) ;
#92420=PLANE ( 'NONE',  #90146 ) ;
#92421=VECTOR ( 'NONE', #12046, 1000.000000000000114 ) ;
#92422=B_SPLINE_CURVE_WITH_KNOTS ( 'NONE', 3,
 ( #30085, #14353, #45331, #77741 ),
 .UNSPECIFIED., .F., .F.,
 ( 4, 4 ),
 ( 0.000000000000000000, 9.999999999998897304E-05 ),
 .UNSPECIFIED. ) ;
#92424=ORIENTED_EDGE ( 'NONE', *, *, #52677, .F. ) ;
#92427=CARTESIAN_POINT ( 'NONE',  ( -81.61611000704998276, -25.23679622552714008, 6.293943003980941420 ) ) ;
#92430=CARTESIAN_POINT ( 'NONE',  ( -58.92287095715003886, -23.47593901973090169, -1.443836447538997758 ) ) ;
#92431=CARTESIAN_POINT ( 'NONE',  ( -30.64752034897746924, -23.47593901973090169, -1.443836447538997758 ) ) ;
#92432=CARTESIAN_POINT ( 'NONE',  ( 1.534201407001029027, 19.92515851932037663, 11.49999999999998934 ) ) ;
#92433=CARTESIAN_POINT ( 'NONE',  ( -95.52287095715010423, -25.00182538069145366, 7.747789668545101982 ) ) ;
#92434=CARTESIAN_POINT ( 'NONE',  ( -45.57564872872666939, -24.92592662359561118, 8.075495903018000021 ) ) ;
#92437=CARTESIAN_POINT ( 'NONE',  ( -109.7896840091628832, -25.29012758118892634, 3.444317882821586796 ) ) ;
#92438=DIRECTION ( 'NONE',  ( 0.000000000000000000, -0.9999999999976377785, -2.173523156925979128E-06 ) ) ;
#92439=CARTESIAN_POINT ( 'NONE',  ( -101.6814946224345704, -25.25287247409163527, 6.236250661346386615 ) ) ;
#92441=B_SPLINE_CURVE_WITH_KNOTS ( 'NONE', 3,
 ( #18373, #48838, #88896, #56954, #80272, #95998 ),
 .UNSPECIFIED., .F., .F.,
 ( 4, 2, 4 ),
 ( 1.570755371633915156E-05, 0.001396183895866088620, 0.002776660238015838181 ),
 .UNSPECIFIED. ) ;
#92444=CARTESIAN_POINT ( 'NONE',  ( -40.52287095715006870, -23.47596703998600631, 11.44779298504229281 ) ) ;
#92446=CARTESIAN_POINT ( 'NONE',  ( 3.949161919925879172, -19.86910077469890723, 11.49999999999998934 ) ) ;
#92447=CARTESIAN_POINT ( 'NONE',  ( -90.55620429048337883, -23.48783264082478084, -1.443836473390064157 ) ) ;
#92451=CARTESIAN_POINT ( 'NONE',  ( -105.6228709571500559, -29.50250243563736774, 8.947779886222136270 ) ) ;
#92452=CARTESIAN_POINT ( 'NONE',  ( 19.08902475966321788, 6.433202353099247262, -1.500000000000002220 ) ) ;
#92453=CARTESIAN_POINT ( 'NONE',  ( -21.07084664159375009, 0.3847054351051909515, 11.49999999999999645 ) ) ;
#92455=CARTESIAN_POINT ( 'NONE',  ( 21.87352179494074633, -3.179377960941109915, 11.49999999999998934 ) ) ;
#92457=CARTESIAN_POINT ( 'NONE',  ( 19.76637988705548210, 5.604140092158477415, -1.500000000000002220 ) ) ;
#92458=LINE ( 'NONE', #30569, #51167 ) ;
#92459=EDGE_CURVE ( 'NONE', #76499, #45115, #57464, .T. ) ;
#92460=CARTESIAN_POINT ( 'NONE',  ( -53.62287095715003460, -23.73907113216990084, -1.053371485793234807 ) ) ;
#92463=ORIENTED_EDGE ( 'NONE', *, *, #12338, .T. ) ;
#92464=CARTESIAN_POINT ( 'NONE',  ( -126.6228709571500275, -23.48783264082479505, -1.443836473390057051 ) ) ;
#92465=CARTESIAN_POINT ( 'NONE',  ( -130.2562042904833959, -23.47596703998600631, 11.44779298504227860 ) ) ;
#92466=ORIENTED_EDGE ( 'NONE', *, *, #42264, .F. ) ;
#92468=ORIENTED_EDGE ( 'NONE', *, *, #70456, .F. ) ;
#92469=PLANE ( 'NONE',  #92335 ) ;
#92471=CARTESIAN_POINT ( 'NONE',  ( -68.50595449436075057, -24.15620529776627734, 10.23563542870660825 ) ) ;
#92472=CARTESIAN_POINT ( 'NONE',  ( 20.50092990308456464, -2.467789585553555654, -1.500000000000002220 ) ) ;
#92473=CARTESIAN_POINT ( 'NONE',  ( 21.32721141102669193, -3.434809268862642817, 11.49999999999999645 ) ) ;
#92475=EDGE_CURVE ( 'NONE', #922, #76871, #64660, .T. ) ;
#92478=CARTESIAN_POINT ( 'NONE',  ( -11.14805103425725719, -19.39388463112642214, -1.500000000000002220 ) ) ;
#92479=EDGE_CURVE ( 'NONE', #88312, #80762, #21129, .T. ) ;
#92481=CARTESIAN_POINT ( 'NONE',  ( -80.48900664166535535, -25.12205811808326672, 7.101635561061091728 ) ) ;
#92482=CARTESIAN_POINT ( 'NONE',  ( -75.52287095715007581, -23.47596703998600631, 11.44779298504228571 ) ) ;
#92485=CARTESIAN_POINT ( 'NONE',  ( -116.4728709571500360, -25.40558663563427189, 5.000950442582703381 ) ) ;
#92487=CARTESIAN_POINT ( 'NONE',  ( -49.50709656002590719, -23.96169478059712432, 10.65365249895718414 ) ) ;
#92491=CARTESIAN_POINT ( 'NONE',  ( -16.13976855045889636, 13.32451261336467496, -1.500000000000002220 ) ) ;
#92492=ORIENTED_EDGE ( 'NONE', *, *, #59899, .T. ) ;
#92493=CARTESIAN_POINT ( 'NONE',  ( -86.50736880509799676, -24.34968618360934300, 0.1864209137778916336 ) ) ;
#92495=CARTESIAN_POINT ( 'NONE',  ( -128.6228709571499849, -24.50321055353805733, 9.387540953477527594 ) ) ;
#92496=CARTESIAN_POINT ( 'NONE',  ( 20.46717832272283033, -5.532298862796615424, -1.500000000000002220 ) ) ;
#92498=CARTESIAN_POINT ( 'NONE',  ( -60.55620429048339304, -24.99156044556202261, 7.747789690856174083 ) ) ;
#92499=CARTESIAN_POINT ( 'NONE',  ( -35.55620429048339304, -25.00182538069145011, 7.747789668545097541 ) ) ;
#92500=CARTESIAN_POINT ( 'NONE',  ( -8.334044162642690878, 20.12857247364870616, 11.49999999999998934 ) ) ;
#92504=CARTESIAN_POINT ( 'NONE',  ( -15.20188179817220231, 15.67080601223297442, -1.500000000000002220 ) ) ;
#92505=CARTESIAN_POINT ( 'NONE',  ( -71.20541289166536103, -25.24674059646277868, 4.885890097747910943 ) ) ;
#92506=ORIENTED_EDGE ( 'NONE', *, *, #47264, .F. ) ;
#92508=CARTESIAN_POINT ( 'NONE',  ( -123.5895376238167245, -24.65952944569305316, 1.056160979905711894 ) ) ;
#92509=EDGE_CURVE ( 'NONE', #99597, #14044, #40950, .T. ) ;
#92511=ORIENTED_EDGE ( 'NONE', *, *, #39104, .F. ) ;
#92512=EDGE_LOOP ( 'NONE', ( #65354, #88883, #82659, #60878 ) ) ;
#92514=ORIENTED_EDGE ( 'NONE', *, *, #62332, .F. ) ;
#92515=CARTESIAN_POINT ( 'NONE',  ( -44.62287095715004881, -23.94994826722565762, -0.6494450866342738049 ) ) ;
#92516=CARTESIAN_POINT ( 'NONE',  ( -16.84575021678815432, -12.90291372800108505, 11.49999999999998934 ) ) ;
#92517=CARTESIAN_POINT ( 'NONE',  ( -94.63995231824821985, -23.48783264082477373, -1.443836473390087249 ) ) ;
#92518=CARTESIAN_POINT ( 'NONE',  ( -80.29067095681661215, -25.27791970390547860, 7.551389258223609069 ) ) ;
#92520=CARTESIAN_POINT ( 'NONE',  ( -80.62287095715004170, -25.00182538069145721, 7.747789668545097541 ) ) ;
#92522=CARTESIAN_POINT ( 'NONE',  ( -19.24332624019526961, -2.196797614219411443, 11.49999999999998934 ) ) ;
#92523=CARTESIAN_POINT ( 'NONE',  ( -51.59514189427220288, -25.31187621157931034, 5.320822997074797556 ) ) ;
#92525=CARTESIAN_POINT ( 'NONE',  ( -19.30698013599780083, -2.078282243779251637, 11.49999999999999645 ) ) ;
#92526=CARTESIAN_POINT ( 'NONE',  ( -88.52287095715006160, -24.65952944569304606, 1.056160979905700570 ) ) ;
#92527=B_SPLINE_CURVE_WITH_KNOTS ( 'NONE', 3,
 ( #85434, #38760, #46889, #69729 ),
 .UNSPECIFIED., .F., .F.,
 ( 4, 4 ),
 ( 1.328512187993866617E-05, 0.002239812633505373039 ),
 .UNSPECIFIED. ) ;
#92529=EDGE_LOOP ( 'NONE', ( #45321, #93072, #87408, #53971 ) ) ;
#92531=CARTESIAN_POINT ( 'NONE',  ( -59.52287095715005449, -24.35013146730204525, 9.818937971375108376 ) ) ;
#92533=EDGE_CURVE ( 'NONE', #80847, #35458, #59786, .T. ) ;
#92535=CARTESIAN_POINT ( 'NONE',  ( -8.122062702759739850, 17.86989387945112995, 11.49999999999998934 ) ) ;
#92536=CARTESIAN_POINT ( 'NONE',  ( -41.29362909362059497, -25.27806053428773581, 4.684754197744505078 ) ) ;
#92537=ORIENTED_EDGE ( 'NONE', *, *, #858, .F. ) ;
#92538=CARTESIAN_POINT ( 'NONE',  ( 15.64208908530913256, 14.88810259432246852, -1.500000000000002220 ) ) ;
#92540=CARTESIAN_POINT ( 'NONE',  ( -40.62957245546282792, -24.83618233451450052, 1.606449574219539267 ) ) ;
#92544=CARTESIAN_POINT ( 'NONE',  ( -11.96207688724106610, 19.68918167733909641, -1.500000000000002220 ) ) ;
#92545=B_SPLINE_CURVE_WITH_KNOTS ( 'NONE', 3,
 ( #22087, #84000, #14483, #90619 ),
 .UNSPECIFIED., .F., .F.,
 ( 4, 4 ),
 ( 0.000000000000000000, 0.0001000000000000028644 ),
 .UNSPECIFIED. ) ;
#92547=CARTESIAN_POINT ( 'NONE',  ( -55.62287095715004170, -23.47596703998600631, 11.44779298504227505 ) ) ;
#92549=CARTESIAN_POINT ( 'NONE',  ( -121.5901295846091585, -24.15620529776628445, 10.23563542870660115 ) ) ;
#92551=CARTESIAN_POINT ( 'NONE',  ( -111.4457194297752807, -25.10921488884410735, 3.361189062929010429 ) ) ;
#92553=FACE_OUTER_BOUND ( 'NONE', #92529, .T. ) ;
#92554=CARTESIAN_POINT ( 'NONE',  ( 8.615496892348360802, 17.92367856960711947, 11.49999999999998934 ) ) ;
#92555=CARTESIAN_POINT ( 'NONE',  ( -101.3738023147422780, -25.27307239909452008, 3.986250617436227550 ) ) ;
#92556=CARTESIAN_POINT ( 'NONE',  ( 12.93213199337649044, -14.99640713134888692, -1.500000000000002220 ) ) ;
#92557=CARTESIAN_POINT ( 'NONE',  ( -56.57855137815445090, -24.65952944569304250, 1.056160979905696795 ) ) ;
#92559=CARTESIAN_POINT ( 'NONE',  ( -108.6228709571500559, -24.64898659630368627, 1.056161002820831474 ) ) ;
#92561=CARTESIAN_POINT ( 'NONE',  ( -1.268444833121266546, 20.69640364028325052, 11.49999999999999645 ) ) ;
#92562=LINE ( 'NONE', #47906, #79126 ) ;
#92563=FACE_OUTER_BOUND ( 'NONE', #96727, .T. ) ;
#92564=CARTESIAN_POINT ( 'NONE',  ( -2.780358639097238349, 22.57001311929844434, 11.49999999999999645 ) ) ;
#92565=ORIENTED_EDGE ( 'NONE', *, *, #56467, .F. ) ;
#92566=CARTESIAN_POINT ( 'NONE',  ( -60.62287095715004170, -24.92579138211020862, 1.929029949965662238 ) ) ;
#92567=CARTESIAN_POINT ( 'NONE',  ( -52.55620429048338593, -23.47596703998600276, 11.44779298504227505 ) ) ;
#92568=CARTESIAN_POINT ( 'NONE',  ( 20.19498477198788322, 0.2509159868347127231, -1.500000000000002220 ) ) ;
#92569=DIRECTION ( 'NONE',  ( 0.000000000000000000, 2.173523156925980399E-06, -0.9999999999976378895 ) ) ;
#92570=CARTESIAN_POINT ( 'NONE',  ( -45.55620429048339304, -23.48786465467240347, 11.44779295918255002 ) ) ;
#92572=B_SPLINE_CURVE_WITH_KNOTS ( 'NONE', 3,
 ( #93593, #15970, #46435, #76369, #22082, #45949, #38315, #61679 ),
 .UNSPECIFIED., .F., .F.,
 ( 4, 2, 2, 4 ),
 ( -0.001224554619866348015, -0.0002241820295893690029, 0.0007761905606876100087, 0.002776935741241576706 ),
 .UNSPECIFIED. ) ;
#92575=CARTESIAN_POINT ( 'NONE',  ( 2.875404258304424143, 22.71175023210845012, 11.49999999999998934 ) ) ;
#92576=CARTESIAN_POINT ( 'NONE',  ( -50.58832339509404363, -25.18439652211503699, 3.304980435165238983 ) ) ;
#92577=CARTESIAN_POINT ( 'NONE',  ( -19.98381242416700587, 8.274006965216138099, -1.500000000000002220 ) ) ;
#92578=CARTESIAN_POINT ( 'NONE',  ( -123.6243262789347739, -24.34968618360933945, 0.1864209137778903291 ) ) ;
#92579=CARTESIAN_POINT ( 'NONE',  ( -34.55279844800535471, -23.96119346886880663, -0.6495511937831991434 ) ) ;
#92580=CARTESIAN_POINT ( 'NONE',  ( -20.36979505965413395, -4.774807507659313721, 11.49999999999999645 ) ) ;
#92581=ORIENTED_EDGE ( 'NONE', *, *, #98144, .T. ) ;
#92582=CARTESIAN_POINT ( 'NONE',  ( -124.6251027437798484, -23.96119346886880308, -0.6495511937832024740 ) ) ;
#92583=CARTESIAN_POINT ( 'NONE',  ( -20.57682416348112397, 7.868404785394932155, -1.500000000000002220 ) ) ;
#92584=CARTESIAN_POINT ( 'NONE',  ( -33.52287095715006160, -29.50248528299804818, 1.056150453629029817 ) ) ;
#92585=DIRECTION ( 'NONE',  ( -3.773278334453079030E-23, 0.9999999999976377785, 2.173523156925979128E-06 ) ) ;
#92588=CARTESIAN_POINT ( 'NONE',  ( -122.6228709571500417, -23.72773821059536559, 11.05748984161097326 ) ) ;
#92591=EDGE_CURVE ( 'NONE', #71172, #24828, #61033, .T. ) ;
#92592=ORIENTED_EDGE ( 'NONE', *, *, #53326, .F. ) ;
#92593=EDGE_CURVE ( 'NONE', #41731, #43974, #29564, .T. ) ;
#92595=CARTESIAN_POINT ( 'NONE',  ( -71.59683312727963767, -23.96169478059713498, 10.65365249895718058 ) ) ;
#92596=CARTESIAN_POINT ( 'NONE',  ( -83.52287095715006160, -24.64965694238407323, 8.947790433994198267 ) ) ;
#92597=CARTESIAN_POINT ( 'NONE',  ( -36.62906116432126424, -24.51314013834316086, 0.6176544820404111791 ) ) ;
#92598=CARTESIAN_POINT ( 'NONE',  ( -19.64171699416042571, -5.764624264842452384, -1.500000000000002220 ) ) ;
#92599=EDGE_CURVE ( 'NONE', #8718, #33210, #13746, .T. ) ;
#92601=CARTESIAN_POINT ( 'NONE',  ( -99.90834851333848121, -25.30148146617204219, 5.319218632498879273 ) ) ;
#92604=CARTESIAN_POINT ( 'NONE',  ( -21.97457344801873447, 3.670769625195870134, 11.49999999999998934 ) ) ;
#92606=CARTESIAN_POINT ( 'NONE',  ( -79.11611000704996854, -25.20074463982482982, 3.409327697717700278 ) ) ;
#92608=ORIENTED_EDGE ( 'NONE', *, *, #20555, .F. ) ;
#92609=LINE ( 'NONE', #16988, #48487 ) ;
#92610=CARTESIAN_POINT ( 'NONE',  ( -29.60812400815161283, -25.26247736358755702, 6.685403929990477501 ) ) ;
#92611=CARTESIAN_POINT ( 'NONE',  ( -20.74012505511919713, -1.853331690952414013, -1.500000000000002220 ) ) ;
#92613=ORIENTED_EDGE ( 'NONE', *, *, #43739, .T. ) ;
#92616=CARTESIAN_POINT ( 'NONE',  ( -50.71600500446225368, -25.12217856757505530, 7.074609049370240044 ) ) ;
#92617=EDGE_CURVE ( 'NONE', #58438, #67443, #35343, .T. ) ;
#92622=B_SPLINE_CURVE_WITH_KNOTS ( 'NONE', 3,
 ( #14527, #61231, #84541, #85539 ),
 .UNSPECIFIED., .F., .F.,
 ( 4, 4 ),
 ( 0.03981435493391547592, 0.04882078620603082231 ),
 .UNSPECIFIED. ) ;
#92624=( BOUNDED_SURFACE ( )  B_SPLINE_SURFACE ( 3, 1, ( 
 ( #72602, #47762 ),
 ( #10192, #56888 ),
 ( #87819, #79696 ),
 ( #72106, #26420 ) ),
 .UNSPECIFIED., .F., .F., .T. ) 
 B_SPLINE_SURFACE_WITH_KNOTS ( ( 4, 4 ),
 ( 2, 2 ),
 ( 0.000000000000000000, 1.000000000000000000 ),
 ( 0.000000000000000000, 1.000000000000000000 ),
 .UNSPECIFIED. ) 
 GEOMETRIC_REPRESENTATION_ITEM ( )  RATIONAL_B_SPLINE_SURFACE ( (
 ( 1.000000000000000000, 1.000000000000000000),
 ( 0.3333333333333333703, 0.3333333333333333703),
 ( 0.3333333333333333703, 0.3333333333333333703),
 ( 1.000000000000000000, 1.000000000000000000) ) ) 
 REPRESENTATION_ITEM ( '' )  SURFACE ( )  );
#92627=CARTESIAN_POINT ( 'NONE',  ( -92.59761174911608350, -23.73791477778911840, 11.05961554403170588 ) ) ;
#92628=CARTESIAN_POINT ( 'NONE',  ( -53.58953762381672448, -23.48783264082478084, -1.443836473390070596 ) ) ;
#92629=CARTESIAN_POINT ( 'NONE',  ( 18.11909884760711975, -12.84011383348296853, 11.49999999999999645 ) ) ;
#92631=CARTESIAN_POINT ( 'NONE',  ( -89.49044893904931541, -25.11033443465437287, 2.832404802291436319 ) ) ;
#92632=ORIENTED_EDGE ( 'NONE', *, *, #34119, .T. ) ;
#92633=CARTESIAN_POINT ( 'NONE',  ( -6.441999407266626676, 21.70310835763521595, 11.49999999999998934 ) ) ;
#92634=CARTESIAN_POINT ( 'NONE',  ( -115.5589197295127946, -23.48786465467241769, 11.44779295918253581 ) ) ;
#92637=ORIENTED_EDGE ( 'NONE', *, *, #92864, .F. ) ;
#92640=CARTESIAN_POINT ( 'NONE',  ( -15.22981678846565856, -13.14137338692033907, -1.500000000000002220 ) ) ;
#92642=VERTEX_POINT ( 'NONE', #36836 ) ;
#92643=CARTESIAN_POINT ( 'NONE',  ( -92.52287095715006160, -23.48786465467241769, 11.44779295918254292 ) ) ;
#92644=CARTESIAN_POINT ( 'NONE',  ( 20.23429811176546167, 9.490607074118958764, -1.500000000000002220 ) ) ;
#92645=ORIENTED_EDGE ( 'NONE', *, *, #83658, .T. ) ;
#92646=ORIENTED_EDGE ( 'NONE', *, *, #4902, .T. ) ;
#92648=CARTESIAN_POINT ( 'NONE',  ( -119.6228709571500559, -24.64965695001469115, 8.947790433994175174 ) ) ;
#92650=PLANE ( 'NONE',  #88734 ) ;
#92653=CARTESIAN_POINT ( 'NONE',  ( 10.86043079284791091, -16.25897383129715834, -1.500000000000002220 ) ) ;
#92654=FACE_OUTER_BOUND ( 'NONE', #98016, .T. ) ;
#92655=CARTESIAN_POINT ( 'NONE',  ( 19.19993882694861753, 9.668096177433461946, -1.500000000000002220 ) ) ;
#92658=CARTESIAN_POINT ( 'NONE',  ( -129.5228709571500474, -24.66019654487199730, 8.947790411086115725 ) ) ;
#92661=CARTESIAN_POINT ( 'NONE',  ( 18.88093902437788785, 12.95799798663108682, -1.500000000000002220 ) ) ;
#92662=VECTOR ( 'NONE', #87537, 1000.000000000000114 ) ;
#92665=CARTESIAN_POINT ( 'NONE',  ( -29.52287095715006160, -24.56560739788454129, 1.056161319240904728 ) ) ;
#92666=CARTESIAN_POINT ( 'NONE',  ( 3.179702300980958185, 19.78100630842630281, 11.49999999999999645 ) ) ;
#92667=CARTESIAN_POINT ( 'NONE',  ( -79.09669456484505190, -25.26612537777918632, 5.260500027664780198 ) ) ;
#92668=CARTESIAN_POINT ( 'NONE',  ( -33.62287095715005592, -23.47596703998600276, 11.44779298504227505 ) ) ;
#92669=PLANE ( 'NONE',  #24667 ) ;
#92672=PLANE ( 'NONE',  #73666 ) ;
#92674=CARTESIAN_POINT ( 'NONE',  ( -19.25911440464646063, 10.06369110047026538, 11.49999999999998934 ) ) ;
#92676=CARTESIAN_POINT ( 'NONE',  ( -18.23851433863309879, 7.102826447048048664, -1.500000000000002220 ) ) ;
#92677=PLANE ( 'NONE',  #50794 ) ;
#92680=CARTESIAN_POINT ( 'NONE',  ( -91.51200254185937411, -24.15620529776628445, 10.23563542870660292 ) ) ;
#92682=CARTESIAN_POINT ( 'NONE',  ( 19.76637988705548210, 5.604140092158477415, 11.49999999999999645 ) ) ;
#92685=CARTESIAN_POINT ( 'NONE',  ( -120.6267774785480356, -24.15503026093913874, -0.2815557561904504791 ) ) ;
#92686=ORIENTED_EDGE ( 'NONE', *, *, #37414, .T. ) ;
#92687=CARTESIAN_POINT ( 'NONE',  ( -99.55666892486131303, -25.31296331729878446, 4.188639739155572528 ) ) ;
#92688=DIRECTION ( 'NONE',  ( -3.773278334444167608E-23, 1.000000000000000000, 0.000000000000000000 ) ) ;
#92689=CARTESIAN_POINT ( 'NONE',  ( -125.5549464543417884, -24.52399227489127043, 9.353111116836528183 ) ) ;
#92691=CARTESIAN_POINT ( 'NONE',  ( -25.74405688418818272, -24.61459765063332483, 6.647229985634355742 ) ) ;
#92693=AXIS2_PLACEMENT_3D ( 'NONE', #77662, #39111, #70065 ) ;
#92694=CARTESIAN_POINT ( 'NONE',  ( -17.14199295335891904, -15.44578658782692671, 11.49999999999999645 ) ) ;
#92695=CARTESIAN_POINT ( 'NONE',  ( -0.9063223138645676302, -22.79912562917415997, -1.500000000000002220 ) ) ;
#92696=CARTESIAN_POINT ( 'NONE',  ( -74.59647204067105974, -23.96119346886880308, -0.6495511937832119109 ) ) ;
#92697=CARTESIAN_POINT ( 'NONE',  ( -78.62287095715005592, -29.50250243563736774, 8.947779886222141599 ) ) ;
#92698=CARTESIAN_POINT ( 'NONE',  ( -86.52287095715000476, -23.95044443724992789, 10.65354141964649237 ) ) ;
#92700=CARTESIAN_POINT ( 'NONE',  ( 18.65981798208652265, 12.38953945867474360, 11.49999999999999645 ) ) ;
#92701=ORIENTED_EDGE ( 'NONE', *, *, #348, .F. ) ;
#92702=CARTESIAN_POINT ( 'NONE',  ( -59.56094173781918499, -29.50249039766296022, 3.409318347773680369 ) ) ;
#92703=CARTESIAN_POINT ( 'NONE',  ( -43.56067006883019843, -23.73766607897671221, -1.055555164236442689 ) ) ;
#92704=CARTESIAN_POINT ( 'NONE',  ( 17.58553779993395594, 13.13030503331179411, 11.49999999999998934 ) ) ;
#92705=CARTESIAN_POINT ( 'NONE',  ( -113.5228709571500616, -24.34917612406836795, 0.1852690917426624284 ) ) ;
#92707=CARTESIAN_POINT ( 'NONE',  ( -33.52287095715004739, -23.73934037231756022, 11.05740245334329686 ) ) ;
#92708=CARTESIAN_POINT ( 'NONE',  ( -69.52287095715006160, -24.64898659630367916, 1.056161002820824368 ) ) ;
#92709=CARTESIAN_POINT ( 'NONE',  ( -96.92287095715008149, -23.47593901973090169, -1.443836447538996870 ) ) ;
#92710=ORIENTED_EDGE ( 'NONE', *, *, #71105, .F. ) ;
#92712=CARTESIAN_POINT ( 'NONE',  ( -4.979992623568794130, 19.86841884474198494, -1.500000000000002220 ) ) ;
#92714=ORIENTED_EDGE ( 'NONE', *, *, #11334, .T. ) ;
#92715=ORIENTED_EDGE ( 'NONE', *, *, #100143, .T. ) ;
#92716=ORIENTED_EDGE ( 'NONE', *, *, #10623, .F. ) ;
#92717=CARTESIAN_POINT ( 'NONE',  ( -18.41700849636773540, 13.91914711744011157, 11.49999999999998934 ) ) ;
#92718=CARTESIAN_POINT ( 'NONE',  ( -40.11481023079474539, -25.30977039686255026, 4.487062071701387822 ) ) ;
#92719=CARTESIAN_POINT ( 'NONE',  ( -20.02346298389695534, -3.155783441878276196, -1.500000000000002220 ) ) ;
#92720=EDGE_CURVE ( 'NONE', #34175, #22695, #96078, .T. ) ;
#92722=CARTESIAN_POINT ( 'NONE',  ( -26.07767875451820316, -24.95303847834740907, 4.027978703335532096 ) ) ;
#92723=CARTESIAN_POINT ( 'NONE',  ( -92.58614606148624659, -24.51314013834316796, 0.6176544820404266112 ) ) ;
#92724=EDGE_CURVE ( 'NONE', #41093, #68328, #73896, .T. ) ;
#92726=CARTESIAN_POINT ( 'NONE',  ( -70.49292501847948245, -24.73486907724917572, 1.287355809206963908 ) ) ;
#92727=CARTESIAN_POINT ( 'NONE',  ( 16.48747857468482891, 13.79107804547330929, 11.49999999999999645 ) ) ;
#92728=EDGE_LOOP ( 'NONE', ( #44558, #38174, #21607, #77898 ) ) ;
#92730=CARTESIAN_POINT ( 'NONE',  ( -34.62287095715007723, -23.94994826722565762, -0.6494450866342736939 ) ) ;
#92732=ORIENTED_EDGE ( 'NONE', *, *, #24145, .F. ) ;
#92734=CARTESIAN_POINT ( 'NONE',  ( 20.29938135082171158, -4.300543036493735372, -1.500000000000002220 ) ) ;
#92735=ORIENTED_EDGE ( 'NONE', *, *, #12541, .T. ) ;
#92736=PLANE ( 'NONE',  #36163 ) ;
#92737=EDGE_LOOP ( 'NONE', ( #58214, #22902, #35436, #98250 ) ) ;
#92739=B_SPLINE_SURFACE_WITH_KNOTS ( 'NONE', 3, 3, ( 
 ( #90453, #20932, #82340, #51905 ),
 ( #37168, #43790, #36666, #67631 ),
 ( #36176, #83334, #98552, #45287 ),
 ( #98052, #29048, #44789, #60523 ),
 ( #60023, #76213, #52397, #61014 ),
 ( #91438, #99046, #21921, #14811 ),
 ( #59517, #52900, #6708, #37663 ) ),
 .UNSPECIFIED., .F., .F., .F.,
 ( 4, 3, 4 ),
 ( 4, 4 ),
 ( 0.0004766839783814116297, 0.1029713700210891786, 0.2054660560637969480 ),
 ( 0.9097254158518339739, 0.9111578860431817084 ),
 .UNSPECIFIED. ) ;
#92741=ORIENTED_EDGE ( 'NONE', *, *, #27731, .F. ) ;
#92742=VERTEX_POINT ( 'NONE', #27229 ) ;
#92743=CARTESIAN_POINT ( 'NONE',  ( -55.52287095715006870, -23.47596703998600631, 11.44779298504228926 ) ) ;
#92744=CARTESIAN_POINT ( 'NONE',  ( -117.2228709571500644, -23.47596703998600631, 11.44779298504227860 ) ) ;
#92746=CARTESIAN_POINT ( 'NONE',  ( -102.5228709571500474, -24.50321055353806088, 9.387540953477520489 ) ) ;
#92747=CARTESIAN_POINT ( 'NONE',  ( -4.809782828112996178, 21.40371668077904488, 11.49999999999999645 ) ) ;
#92748=CARTESIAN_POINT ( 'NONE',  ( 20.50669422456317292, -9.396423750077818937, -1.500000000000002220 ) ) ;
#92749=CARTESIAN_POINT ( 'NONE',  ( -12.59924929152775874, 16.77720732749412846, 11.49999999999998934 ) ) ;
#92750=FACE_OUTER_BOUND ( 'NONE', #62394, .T. ) ;
#92751=FACE_OUTER_BOUND ( 'NONE', #13220, .T. ) ;
#92752=VERTEX_POINT ( 'NONE', #4395 ) ;
#92753=AXIS2_PLACEMENT_3D ( 'NONE', #34294, #33787, #26171 ) ;
#92754=ORIENTED_EDGE ( 'NONE', *, *, #8212, .T. ) ;
#92755=ORIENTED_EDGE ( 'NONE', *, *, #81277, .T. ) ;
#92756=B_SPLINE_CURVE_WITH_KNOTS ( 'NONE', 3,
 ( #16091, #7982, #8982, #48057, #16585, #78986 ),
 .UNSPECIFIED., .F., .F.,
 ( 4, 2, 4 ),
 ( 0.000000000000000000, 0.001380901958385389412, 0.002761803916770778824 ),
 .UNSPECIFIED. ) ;
#92757=CARTESIAN_POINT ( 'NONE',  ( -36.62287095715005592, -24.34917612406837861, 0.1852690917426571271 ) ) ;
#92758=CARTESIAN_POINT ( 'NONE',  ( -10.19830463584622571, -18.94658877215714909, -1.500000000000002220 ) ) ;
#92759=CARTESIAN_POINT ( 'NONE',  ( -85.52287095715004739, -29.50249982740957577, 7.747779886224967605 ) ) ;
#92760=ORIENTED_EDGE ( 'NONE', *, *, #13019, .F. ) ;
#92761=CARTESIAN_POINT ( 'NONE',  ( 6.572693220633653688, -20.11273663914708365, 11.49999999999998934 ) ) ;
#92762=CARTESIAN_POINT ( 'NONE',  ( -96.62287095715005592, -29.50248528299804818, 1.056150453629042030 ) ) ;
#92763=CARTESIAN_POINT ( 'NONE',  ( -50.46940435010577630, -25.26041116785443563, 7.561691964516831455 ) ) ;
#92764=CARTESIAN_POINT ( 'NONE',  ( -121.5222464850925661, -23.48783264082477373, -1.443836473390087916 ) ) ;
#92765=DIRECTION ( 'NONE',  ( -1.000000000000000000, -3.773278334444167608E-23, -8.201307833595939069E-29 ) ) ;
#92766=CARTESIAN_POINT ( 'NONE',  ( -101.5228709571500758, -24.51283580621364777, 0.6167428607019801445 ) ) ;
#92767=CARTESIAN_POINT ( 'NONE',  ( 5.777647480883832287, 21.37485705712154171, -1.500000000000002220 ) ) ;
#92768=CARTESIAN_POINT ( 'NONE',  ( -81.52213703500444808, -23.48786465467241058, 11.44779295918254824 ) ) ;
#92769=EDGE_CURVE ( 'NONE', #24715, #11225, #27067, .T. ) ;
#92770=B_SPLINE_CURVE_WITH_KNOTS ( 'NONE', 3,
 ( #63418, #14822, #61529, #69117, #71017, #30048 ),
 .UNSPECIFIED., .F., .F.,
 ( 4, 2, 4 ),
 ( 1.570887131794638196E-05, 0.001396322306279762591, 0.002776935741241578874 ),
 .UNSPECIFIED. ) ;
#92772=CARTESIAN_POINT ( 'NONE',  ( -82.55620429048336462, -23.47596703998600276, 11.44779298504227683 ) ) ;
#92773=CARTESIAN_POINT ( 'NONE',  ( -110.6228709571500559, -29.50250786944525672, 11.44777988621622988 ) ) ;
#92774=CARTESIAN_POINT ( 'NONE',  ( -2.960655606634402748, -19.13016773636607581, 11.49999999999999645 ) ) ;
#92775=EDGE_CURVE ( 'NONE', #70435, #69536, #6578, .T. ) ;
#92776=CARTESIAN_POINT ( 'NONE',  ( -100.5053578517286326, -24.92564183028979130, 1.928384488918251760 ) ) ;
#92778=CARTESIAN_POINT ( 'NONE',  ( 19.33761327413411024, 2.027444641817329973, -1.500000000000002220 ) ) ;
#92780=CARTESIAN_POINT ( 'NONE',  ( -11.99125074976391048, 17.70416384622758343, 11.49999999999998934 ) ) ;
#92784=CARTESIAN_POINT ( 'NONE',  ( -107.6228709571500701, -23.47593901973091235, -1.443836447538999312 ) ) ;
#92785=CARTESIAN_POINT ( 'NONE',  ( -7.973561950239375307, 21.24132968703115765, -1.500000000000002220 ) ) ;
#92789=CARTESIAN_POINT ( 'NONE',  ( -122.5562042904833646, -23.48783264082479505, -1.443836473390057717 ) ) ;
#92790=CARTESIAN_POINT ( 'NONE',  ( -18.24115112668064853, 7.888873183027880209, 11.49999999999999645 ) ) ;
#92793=ORIENTED_EDGE ( 'NONE', *, *, #29868, .F. ) ;
#92798=CARTESIAN_POINT ( 'NONE',  ( 1.064956243273112557, 21.61254047163424019, -1.500000000000002220 ) ) ;
#92800=CARTESIAN_POINT ( 'NONE',  ( -13.55963120218723361, -13.89248740512243430, -1.500000000000002220 ) ) ;
#92802=CARTESIAN_POINT ( 'NONE',  ( -55.62594644532315868, -24.92592662359560762, 8.075495903017996469 ) ) ;
#92803=CARTESIAN_POINT ( 'NONE',  ( 18.55763160240848109, 7.024834138330111166, -1.500000000000002220 ) ) ;
#92805=CARTESIAN_POINT ( 'NONE',  ( 5.487062353440709472, 19.58251264919930534, 11.49999999999999645 ) ) ;
#92806=CARTESIAN_POINT ( 'NONE',  ( -80.58144820728932700, -24.92564183028979130, 1.928384488918253536 ) ) ;
#92809=B_SPLINE_CURVE_WITH_KNOTS ( 'NONE', 3,
 ( #48510, #54124, #78431, #87055 ),
 .UNSPECIFIED., .F., .F.,
 ( 4, 4 ),
 ( 0.000000000000000000, 1.000000000000000000 ),
 .UNSPECIFIED. ) ;
#92811=CARTESIAN_POINT ( 'NONE',  ( -102.5870824237361489, -24.51419770103155926, 9.386484678747178734 ) ) ;
#92813=CARTESIAN_POINT ( 'NONE',  ( -48.87629837916329478, -25.25214667544315716, 6.044965762095690032 ) ) ;
#92814=CARTESIAN_POINT ( 'NONE',  ( -40.54153813899623060, -24.40133493613049609, 9.663955038902802386 ) ) ;
#92815=B_SPLINE_CURVE_WITH_KNOTS ( 'NONE', 3,
 ( #27518, #80615, #57308, #24823, #87736, #80115, #18221, #49191 ),
 .UNSPECIFIED., .F., .F.,
 ( 4, 2, 2, 4 ),
 ( -0.001224873891641418272, -0.0002244903592271035083, 0.0007758931731872112554, 0.002776660238015837313 ),
 .UNSPECIFIED. ) ;
#92816=CARTESIAN_POINT ( 'NONE',  ( -81.92287095715008149, -23.47596703998600631, 11.44779298504227860 ) ) ;
#92817=CARTESIAN_POINT ( 'NONE',  ( 20.09017895974002599, 0.4902201509063087159, -1.500000000000002220 ) ) ;
#92819=AXIS2_PLACEMENT_3D ( 'NONE', #19611, #34851, #89139 ) ;
#92821=CARTESIAN_POINT ( 'NONE',  ( -30.64427850938831099, -23.56000036390796382, 11.50200000000000067 ) ) ;
#92822=CARTESIAN_POINT ( 'NONE',  ( 11.15996004898972771, 19.99216496293481882, 11.49999999999999645 ) ) ;
#92823=CARTESIAN_POINT ( 'NONE',  ( 17.68435195917723490, -14.24712819257710095, 11.49999999999998934 ) ) ;
#92824=ORIENTED_EDGE ( 'NONE', *, *, #45043, .F. ) ;
#92825=CARTESIAN_POINT ( 'NONE',  ( -45.52287095715006160, -23.85196035786899316, -0.8779234886475214550 ) ) ;
#92828=CARTESIAN_POINT ( 'NONE',  ( -38.50503708857883822, -23.96169478059712432, 10.65365249895718591 ) ) ;
#92829=CARTESIAN_POINT ( 'NONE',  ( -30.57287095715006586, -25.23631683304001072, 3.591709287666025485 ) ) ;
#92833=CARTESIAN_POINT ( 'NONE',  ( 20.35419724272142616, 1.316291261081859787, 11.49999999999998934 ) ) ;
#92834=ORIENTED_EDGE ( 'NONE', *, *, #6973, .F. ) ;
#92835=EDGE_CURVE ( 'NONE', #82610, #27537, #84033, .T. ) ;
#92836=CARTESIAN_POINT ( 'NONE',  ( 20.04565040668967413, 11.27863464804978477, -1.500000000000002220 ) ) ;
#92837=CARTESIAN_POINT ( 'NONE',  ( -88.52287095715006160, -23.47593901973090524, -1.443836447538996426 ) ) ;
#92838=ORIENTED_EDGE ( 'NONE', *, *, #28946, .T. ) ;
#92839=CARTESIAN_POINT ( 'NONE',  ( -101.6228709571501270, -24.33927499327855060, 9.819080762295810061 ) ) ;
#92840=CARTESIAN_POINT ( 'NONE',  ( -81.30502697372733678, -25.19369771803663127, 6.720958911583400308 ) ) ;
#92842=B_SPLINE_CURVE_WITH_KNOTS ( 'NONE', 3,
 ( #22547, #92077, #69750, #232, #31174, #65662 ),
 .UNSPECIFIED., .F., .F.,
 ( 4, 2, 4 ),
 ( 0.000000000000000000, 0.001380901958385388545, 0.002761803916770777089 ),
 .UNSPECIFIED. ) ;
#92843=CARTESIAN_POINT ( 'NONE',  ( -51.52205495810211033, -23.48786465467241058, 11.44779295918254824 ) ) ;
#92844=CARTESIAN_POINT ( 'NONE',  ( 13.48273455363431772, -16.43370779934446801, 11.49999999999999645 ) ) ;
#92845=EDGE_LOOP ( 'NONE', ( #88520, #4369, #30602, #43167 ) ) ;
#92846=VERTEX_POINT ( 'NONE', #94367 ) ;
#92847=EDGE_CURVE ( 'NONE', #83417, #53379, #42896, .T. ) ;
#92848=ORIENTED_EDGE ( 'NONE', *, *, #40427, .F. ) ;
#92849=CARTESIAN_POINT ( 'NONE',  ( 0.7529269182969693386, -22.20201975079678647, 11.49999999999998934 ) ) ;
#92850=ADVANCED_FACE ( 'NONE', ( #22081 ), #38033, .T. ) ;
#92851=CARTESIAN_POINT ( 'NONE',  ( -11.86786554430972096, -16.85652113839894639, 11.49999999999998934 ) ) ;
#92856=CARTESIAN_POINT ( 'NONE',  ( -95.50253988115005654, -24.92592662359561473, 8.075495903017998245 ) ) ;
#92858=CARTESIAN_POINT ( 'NONE',  ( -91.54409941458948197, -24.65952944569304606, 1.056160979905703234 ) ) ;
#92859=ORIENTED_EDGE ( 'NONE', *, *, #794, .F. ) ;
#92862=CARTESIAN_POINT ( 'NONE',  ( -96.52287095715006160, -29.50248528299804818, 1.056150453629042030 ) ) ;
#92863=CARTESIAN_POINT ( 'NONE',  ( -20.61801493038525379, 2.926015819835423581, -1.500000000000002220 ) ) ;
#92864=EDGE_CURVE ( 'NONE', #32116, #28525, #79176, .T. ) ;
#92865=CARTESIAN_POINT ( 'NONE',  ( 6.392671032147439369, 20.83241601264130693, 11.49999999999999645 ) ) ;
#92868=CARTESIAN_POINT ( 'NONE',  ( -22.46026885398333661, -0.8929446408661095846, 11.49999999999998934 ) ) ;
#92869=FACE_OUTER_BOUND ( 'NONE', #31851, .T. ) ;
#92874=VERTEX_POINT ( 'NONE', #83491 ) ;
#92876=ORIENTED_EDGE ( 'NONE', *, *, #19334, .F. ) ;
#92877=CARTESIAN_POINT ( 'NONE',  ( 16.11712757473013014, 13.99349609535929773, -1.500000000000002220 ) ) ;
#92878=ORIENTED_EDGE ( 'NONE', *, *, #72802, .F. ) ;
#92879=CARTESIAN_POINT ( 'NONE',  ( 16.43158684610488862, 13.14696595092960152, -1.500000000000002220 ) ) ;
#92880=CARTESIAN_POINT ( 'NONE',  ( -30.56647679783655036, -24.05295578312052385, -0.4713115009884515927 ) ) ;
#92881=CARTESIAN_POINT ( 'NONE',  ( -114.5228709571500616, -29.50248528299804818, 1.056150453629043584 ) ) ;
#92883=CARTESIAN_POINT ( 'NONE',  ( -18.27885182143903720, 12.20952002138517045, -1.500000000000002220 ) ) ;
#92884=CARTESIAN_POINT ( 'NONE',  ( -76.62287095715007013, -24.65952944569304606, 1.056160979905700126 ) ) ;
#92886=DIRECTION ( 'NONE',  ( -3.773278334453080206E-23, 0.9999999999976377785, 2.173523156925979975E-06 ) ) ;
#92888=CARTESIAN_POINT ( 'NONE',  ( -125.6228709571500559, -29.50248789122583659, 2.256150453626215580 ) ) ;
#92889=CARTESIAN_POINT ( 'NONE',  ( -20.74012505511919713, -1.853331690952414013, 11.49999999999999645 ) ) ;
#92892=AXIS2_PLACEMENT_3D ( 'NONE', #82949, #46397, #22536 ) ;
#92894=CARTESIAN_POINT ( 'NONE',  ( -10.26553491520735406, -22.69622746286980330, 9.960784317162939772 ) ) ;
#92895=CARTESIAN_POINT ( 'NONE',  ( -9.338289970059909351, 19.12570833482435617, 11.49999999999998934 ) ) ;
#92896=CARTESIAN_POINT ( 'NONE',  ( -98.59358047865015351, -23.96169478059713853, 10.65365249895717881 ) ) ;
#92898=CARTESIAN_POINT ( 'NONE',  ( -90.62287095715002749, -23.84047902841601640, -0.8780736468305799791 ) ) ;
#92899=CARTESIAN_POINT ( 'NONE',  ( -69.99198265981809186, -25.28687673834294003, 5.910757521653128066 ) ) ;
#92900=CARTESIAN_POINT ( 'NONE',  ( -14.39138815452349718, -17.32352244779961481, -1.500000000000002220 ) ) ;
#92901=EDGE_CURVE ( 'NONE', #7329, #11431, #28318, .T. ) ;
#92902=CARTESIAN_POINT ( 'NONE',  ( -110.9414999475800272, -25.06174035403189038, 7.474877196992074424 ) ) ;
#92903=ORIENTED_EDGE ( 'NONE', *, *, #85452, .T. ) ;
#92905=CARTESIAN_POINT ( 'NONE',  ( 9.507684299284662188, -17.14340340408069707, 11.49999999999999645 ) ) ;
#92906=CARTESIAN_POINT ( 'NONE',  ( -125.6228709571500559, -24.52232992886361274, 0.6492154411906163602 ) ) ;
#92907=CARTESIAN_POINT ( 'NONE',  ( -32.52287095715006160, -24.51387760970726504, 9.387446482453436047 ) ) ;
#92908=ORIENTED_EDGE ( 'NONE', *, *, #38443, .T. ) ;
#92909=FACE_OUTER_BOUND ( 'NONE', #37732, .T. ) ;
#92910=DIRECTION ( 'NONE',  ( -3.773278334453079618E-23, 0.9999999999976377785, 2.173523156925979975E-06 ) ) ;
#92911=CARTESIAN_POINT ( 'NONE',  ( -88.86953192292943982, -25.31476272485208057, 5.144091107239471938 ) ) ;
#92912=VECTOR ( 'NONE', #55473, 1000.000000000000114 ) ;
#92913=CARTESIAN_POINT ( 'NONE',  ( 15.11087362536062173, -12.71848776332401521, -1.500000000000002220 ) ) ;
#92916=EDGE_CURVE ( 'NONE', #23124, #59212, #1730, .T. ) ;
#92917=EDGE_CURVE ( 'NONE', #37981, #57842, #68282, .T. ) ;
#92923=CARTESIAN_POINT ( 'NONE',  ( -81.75072539166535535, -25.23679622552714363, 6.293943003980942308 ) ) ;
#92928=CARTESIAN_POINT ( 'NONE',  ( -29.62287095715004881, -23.39678932012542845, -1.443836140311830940 ) ) ;
#92929=CARTESIAN_POINT ( 'NONE',  ( 18.25133680241413359, 8.160682379734268466, 11.49999999999998934 ) ) ;
#92930=DIRECTION ( 'NONE',  ( -0.000000000000000000, 2.173523156925979552E-06, -0.9999999999976378895 ) ) ;
#92931=CARTESIAN_POINT ( 'NONE',  ( -51.66817263684756512, -25.29162628464893103, 4.237763228474503485 ) ) ;
#92932=ORIENTED_EDGE ( 'NONE', *, *, #80981, .F. ) ;
#92933=EDGE_CURVE ( 'NONE', #21, #46348, #51331, .T. ) ;
#92935=CARTESIAN_POINT ( 'NONE',  ( -79.50173439926879837, -24.51419770103157347, 9.386484678747176957 ) ) ;
#92936=CARTESIAN_POINT ( 'NONE',  ( -109.6228709571500559, -29.50250786944525672, 11.44777988621622988 ) ) ;
#92937=CARTESIAN_POINT ( 'NONE',  ( -35.61370564495084778, -23.85016227208580730, -0.8807180028928173199 ) ) ;
#92938=CARTESIAN_POINT ( 'NONE',  ( -101.9507253916653440, -25.25287247409162816, 6.236250661346385726 ) ) ;
#92943=DIRECTION ( 'NONE',  ( 0.000000000000000000, 2.173523156925980399E-06, -0.9999999999976378895 ) ) ;
#92944=ORIENTED_EDGE ( 'NONE', *, *, #45900, .T. ) ;
#92945=CARTESIAN_POINT ( 'NONE',  ( 20.23811035156253979, -1.552196809741442696, 11.49999999999998934 ) ) ;
#92948=VECTOR ( 'NONE', #32111, 1000.000000000000114 ) ;
#92951=CARTESIAN_POINT ( 'NONE',  ( -86.52287095715009002, -24.35013146730204170, 9.818937971375103047 ) ) ;
#92952=CARTESIAN_POINT ( 'NONE',  ( -19.48533387766964964, -5.011242947278518045, -1.500000000000002220 ) ) ;
#92953=VECTOR ( 'NONE', #77977, 1000.000000000000114 ) ;
#92954=CARTESIAN_POINT ( 'NONE',  ( -14.90395405082875335, 14.90835605916499418, 11.49999999999999645 ) ) ;
#92955=CARTESIAN_POINT ( 'NONE',  ( 2.710298230372018669, -21.94706154713207980, -1.500000000000002220 ) ) ;
#92957=CARTESIAN_POINT ( 'NONE',  ( -20.41219973434085944, 2.133827299322149429, 11.49999999999998934 ) ) ;
#92958=CARTESIAN_POINT ( 'NONE',  ( -59.66800995418955722, -25.32911129577617970, 4.489957709566354538 ) ) ;
#92959=CARTESIAN_POINT ( 'NONE',  ( -60.56964333814166679, -23.48783264082477018, -1.443836473390097908 ) ) ;
#92960=VERTEX_POINT ( 'NONE', #2774 ) ;
#92962=ORIENTED_EDGE ( 'NONE', *, *, #52422, .T. ) ;
#92965=CARTESIAN_POINT ( 'NONE',  ( -85.62287095715002749, -24.52323809116983000, 9.355190652339416602 ) ) ;
#92966=ORIENTED_EDGE ( 'NONE', *, *, #80816, .T. ) ;
#92968=ORIENTED_EDGE ( 'NONE', *, *, #2020, .F. ) ;
#92969=CARTESIAN_POINT ( 'NONE',  ( -116.6228709571500559, -23.47593901973091235, -1.443836447538997536 ) ) ;
#92970=PLANE ( 'NONE',  #11362 ) ;
#92971=CARTESIAN_POINT ( 'NONE',  ( -68.58386858832108146, -24.51419770103157347, 9.386484678747180510 ) ) ;
#92972=CARTESIAN_POINT ( 'NONE',  ( 20.28538307770854487, 3.844468116359331944, -1.500000000000002220 ) ) ;
#92974=CARTESIAN_POINT ( 'NONE',  ( 17.58597629297885589, -12.55149374826878272, 11.49999999999999645 ) ) ;
#92975=ORIENTED_EDGE ( 'NONE', *, *, #25845, .F. ) ;
#92977=CARTESIAN_POINT ( 'NONE',  ( -60.62287095715006302, -24.91544648472620693, 1.928969306349228363 ) ) ;
#92978=CARTESIAN_POINT ( 'NONE',  ( -15.72835732567950195, 15.92727474065614501, -1.500000000000002220 ) ) ;
#92980=CARTESIAN_POINT ( 'NONE',  ( -47.64622550042292204, -23.96169478059712432, 10.65365249895718591 ) ) ;
#92983=CARTESIAN_POINT ( 'NONE',  ( -58.55620429048338593, -24.65952944569304250, 1.056160979905696129 ) ) ;
#92985=PLANE ( 'NONE',  #84302 ) ;
#92986=CARTESIAN_POINT ( 'NONE',  ( -16.12721948686093754, -13.32240427740599564, 11.49999999999998934 ) ) ;
#92989=ORIENTED_EDGE ( 'NONE', *, *, #99782, .F. ) ;
#92990=CARTESIAN_POINT ( 'NONE',  ( -128.6228709571500701, -23.95044443724992433, 10.65354141964650481 ) ) ;
#92991=CARTESIAN_POINT ( 'NONE',  ( 19.97935793590388442, -6.945280299276400449, -1.500000000000002220 ) ) ;
#92992=B_SPLINE_CURVE_WITH_KNOTS ( 'NONE', 3,
 ( #59768, #52641, #36414, #67377 ),
 .UNSPECIFIED., .F., .F.,
 ( 4, 4 ),
 ( 0.000000000000000000, 9.999999999998206125E-05 ),
 .UNSPECIFIED. ) ;
#92994=CARTESIAN_POINT ( 'NONE',  ( -50.67080217151737287, -23.48783264082476308, -1.443836473390096797 ) ) ;
#92995=CARTESIAN_POINT ( 'NONE',  ( 17.22188757068894915, 13.35947340969901198, -1.500000000000002220 ) ) ;
#92996=PLANE ( 'NONE',  #99957 ) ;
#92997=B_SPLINE_CURVE_WITH_KNOTS ( 'NONE', 3,
 ( #100054, #67659, #51927, #6731 ),
 .UNSPECIFIED., .F., .F.,
 ( 4, 4 ),
 ( 0.6292232213963703247, 0.6302239684371359063 ),
 .UNSPECIFIED. ) ;
#92998=CARTESIAN_POINT ( 'NONE',  ( -41.52287095715006870, -24.64898659630528144, 1.056161002820819261 ) ) ;
#93000=CARTESIAN_POINT ( 'NONE',  ( 17.22188757068894915, 13.35947340969901198, -1.500000000000002220 ) ) ;
#93001=CARTESIAN_POINT ( 'NONE',  ( -95.52287095715011844, -24.52232992886363760, 0.6492154411906031486 ) ) ;
#93002=ORIENTED_EDGE ( 'NONE', *, *, #27568, .F. ) ;
#93003=CARTESIAN_POINT ( 'NONE',  ( -30.54625915432725591, -23.48007831457673689, 11.44779284091286087 ) ) ;
#93005=ORIENTED_EDGE ( 'NONE', *, *, #50792, .F. ) ;
#93006=ORIENTED_EDGE ( 'NONE', *, *, #5024, .T. ) ;
#93007=EDGE_CURVE ( 'NONE', #90387, #44200, #64186, .T. ) ;
#93009=CARTESIAN_POINT ( 'NONE',  ( -29.24566889703875106, -25.20109657442075601, 4.649030501266317117 ) ) ;
#93011=CARTESIAN_POINT ( 'NONE',  ( -4.771770383141621608, -20.67029057396967318, -1.500000000000002220 ) ) ;
#93012=CARTESIAN_POINT ( 'NONE',  ( -121.6228709571500417, -23.47593901973091235, -1.443836447538997536 ) ) ;
#93013=CARTESIAN_POINT ( 'NONE',  ( -79.98156793206884174, -25.27791956405971163, 7.487048666137972042 ) ) ;
#93015=FACE_OUTER_BOUND ( 'NONE', #86153, .T. ) ;
#93016=CARTESIAN_POINT ( 'NONE',  ( -99.52287095715003318, -23.72747288104470087, -1.053458166803225682 ) ) ;
#93017=CARTESIAN_POINT ( 'NONE',  ( 18.67713048845720181, -5.233370074711279685, 11.49999999999998934 ) ) ;
#93019=CARTESIAN_POINT ( 'NONE',  ( -40.93246554024547379, -25.31392318313163514, 5.203682277190879724 ) ) ;
#93020=VERTEX_POINT ( 'NONE', #40324 ) ;
#93021=CARTESIAN_POINT ( 'NONE',  ( 3.148799746435844593, 19.17640706095922098, 11.49999999999999645 ) ) ;
#93025=VECTOR ( 'NONE', #4990, 1000.000000000000114 ) ;
#93027=LINE ( 'NONE', #16915, #20473 ) ;
#93030=CARTESIAN_POINT ( 'NONE',  ( 0.7808950796103379943, -19.64173473864696717, 11.49999999999998934 ) ) ;
#93032=CARTESIAN_POINT ( 'NONE',  ( -41.46379453422112249, -25.31583596542261816, 4.278542312007326487 ) ) ;
#93034=CARTESIAN_POINT ( 'NONE',  ( 5.819084965910729323, 20.79142713412266730, 11.49999999999998934 ) ) ;
#93036=CARTESIAN_POINT ( 'NONE',  ( -40.58888693302551331, -24.52300882791530157, 0.6510814631126359275 ) ) ;
#93037=CARTESIAN_POINT ( 'NONE',  ( -90.52287095715000476, -24.52323809116983355, 9.355190652339423707 ) ) ;
#93038=CARTESIAN_POINT ( 'NONE',  ( -16.13607370526515794, 16.44073208242836159, -1.500000000000002220 ) ) ;
#93041=CARTESIAN_POINT ( 'NONE',  ( -93.62566969909174475, -24.51314013834316086, 0.6176544820404149538 ) ) ;
#93042=CARTESIAN_POINT ( 'NONE',  ( -115.5562042904833788, -23.47593901973091235, -1.443836447538997536 ) ) ;
#93043=CARTESIAN_POINT ( 'NONE',  ( -121.5564787414976990, -23.73791477778912551, 11.05961554403170055 ) ) ;
#93044=DIRECTION ( 'NONE',  ( 0.000000000000000000, 0.9999999999976377785, 2.173523156925979128E-06 ) ) ;
#93045=CARTESIAN_POINT ( 'NONE',  ( -109.5647320221236356, -25.22850916238827068, 3.633130482123976712 ) ) ;
#93046=CARTESIAN_POINT ( 'NONE',  ( -121.6228709571500417, -23.48786465467241769, 11.44779295918253759 ) ) ;
#93047=CARTESIAN_POINT ( 'NONE',  ( -99.64934318012689118, -25.31566098596702119, 4.927356294101793210 ) ) ;
#93048=CARTESIAN_POINT ( 'NONE',  ( 14.69432462292611952, 13.40460087117274490, 11.49999999999998934 ) ) ;
#93049=CARTESIAN_POINT ( 'NONE',  ( -79.11611000704996854, -25.21083105912962097, 3.409327675794633361 ) ) ;
#93050=EDGE_CURVE ( 'NONE', #63968, #42129, #47556, .T. ) ;
#93051=CARTESIAN_POINT ( 'NONE',  ( -5.703961651189128901, -19.02375728206049743, -1.500000000000002220 ) ) ;
#93056=CARTESIAN_POINT ( 'NONE',  ( -39.04979701406145409, -25.29116779651338831, 4.033763859792823148 ) ) ;
#93058=CARTESIAN_POINT ( 'NONE',  ( 5.906898857431191807, -19.90033995357616092, 11.49999999999999645 ) ) ;
#93060=CARTESIAN_POINT ( 'NONE',  ( -126.5562042904833930, -24.64898659630529565, 1.056161002820832806 ) ) ;
#93061=CARTESIAN_POINT ( 'NONE',  ( -16.34568771794417685, -15.85656593008108750, 11.49999999999999645 ) ) ;
#93063=CARTESIAN_POINT ( 'NONE',  ( -69.56520740950848847, -23.48783264082476308, -1.443836473390097908 ) ) ;
#93066=CARTESIAN_POINT ( 'NONE',  ( -19.98115086844608612, 2.773124471107000666, -1.500000000000002220 ) ) ;
#93067=EDGE_CURVE ( 'NONE', #52082, #85110, #48815, .T. ) ;
#93068=ADVANCED_FACE ( 'NONE', ( #32702 ), #95107, .T. ) ;
#93070=CARTESIAN_POINT ( 'NONE',  ( -95.62287095715005592, -24.99132157543084531, 2.256160258750667502 ) ) ;
#93071=B_SPLINE_CURVE_WITH_KNOTS ( 'NONE', 3,
 ( #35451, #11105, #96344, #66420 ),
 .UNSPECIFIED., .F., .F.,
 ( 4, 4 ),
 ( 0.1699072510866937724, 0.1789136823588095560 ),
 .UNSPECIFIED. ) ;
#93072=ORIENTED_EDGE ( 'NONE', *, *, #24145, .T. ) ;
#93073=ORIENTED_EDGE ( 'NONE', *, *, #19135, .F. ) ;
#93076=CARTESIAN_POINT ( 'NONE',  ( -13.69284064830502423, 18.33895024417757469, 11.49999999999998934 ) ) ;
#93077=CARTESIAN_POINT ( 'NONE',  ( -41.51659605236564232, -25.19377129250086611, 3.283922396756908668 ) ) ;
#93078=CARTESIAN_POINT ( 'NONE',  ( 20.17453868081960167, 7.849935799312063089, -1.500000000000002220 ) ) ;
#93079=CARTESIAN_POINT ( 'NONE',  ( -123.5194377984048941, -24.51314013834318217, 0.6176544820404261671 ) ) ;
#93080=CARTESIAN_POINT ( 'NONE',  ( -15.12424899162716230, 14.39509690008720177, 11.49999999999999645 ) ) ;
#93082=CARTESIAN_POINT ( 'NONE',  ( -69.03429854110324015, -25.31612597287615785, 5.665244572013464541 ) ) ;
#93083=CARTESIAN_POINT ( 'NONE',  ( -21.82725030464235516, 2.967780500094957308, -1.500000000000002220 ) ) ;
#93084=AXIS2_PLACEMENT_3D ( 'NONE', #67125, #82326, #66635 ) ;
#93091=VERTEX_POINT ( 'NONE', #34710 ) ;
#93092=CARTESIAN_POINT ( 'NONE',  ( -72.65005370508750104, -23.48786465467241058, 11.44779295918254824 ) ) ;
#93093=VERTEX_POINT ( 'NONE', #28587 ) ;
#93095=CARTESIAN_POINT ( 'NONE',  ( -71.65051242377489871, -23.48786465467241058, 11.44779295918254824 ) ) ;
#93096=CARTESIAN_POINT ( 'NONE',  ( -101.4571681947234083, -25.27404731337933441, 3.296845483386515063 ) ) ;
#93097=CARTESIAN_POINT ( 'NONE',  ( -36.64213287987285383, -24.15543982623907127, -0.2315651400026672579 ) ) ;
#93098=CARTESIAN_POINT ( 'NONE',  ( 19.09590870110849181, 7.302211495713927469, -1.500000000000002220 ) ) ;
#93100=AXIS2_PLACEMENT_3D ( 'NONE', #32337, #77990, #385 ) ;
#93101=EDGE_LOOP ( 'NONE', ( #12991, #57478, #53837, #8295 ) ) ;
#93103=CARTESIAN_POINT ( 'NONE',  ( -44.50617629668793995, -23.96119346886879953, -0.6495511937832129101 ) ) ;
#93104=CARTESIAN_POINT ( 'NONE',  ( -99.55620429048337883, -23.48783264082477729, -1.443836473390061492 ) ) ;
#93105=CARTESIAN_POINT ( 'NONE',  ( 4.546662993595487201, 21.82331882591909178, -1.500000000000002220 ) ) ;
#93108=CARTESIAN_POINT ( 'NONE',  ( -31.52287095715006160, -24.66019654487198665, 8.947790411086131712 ) ) ;
#93112=CARTESIAN_POINT ( 'NONE',  ( -29.81116385467300489, -25.26247379366626333, 5.042945557627021458 ) ) ;
#93113=CARTESIAN_POINT ( 'NONE',  ( 9.770152518076534065, 18.40777400073588410, 11.49999999999998934 ) ) ;
#93116=ORIENTED_EDGE ( 'NONE', *, *, #85849, .F. ) ;
#93118=CARTESIAN_POINT ( 'NONE',  ( -17.04133944854041616, 12.32129857345222845, -1.500000000000002220 ) ) ;
#93120=CARTESIAN_POINT ( 'NONE',  ( -69.52287095715009002, -24.51387760970724727, 9.387446482453405849 ) ) ;
#93121=CARTESIAN_POINT ( 'NONE',  ( -51.29687923781917647, -25.26364009307625125, 3.993462176398971497 ) ) ;
#93123=CARTESIAN_POINT ( 'NONE',  ( -123.6228709571500559, -23.48783264082478794, -1.443836473390058606 ) ) ;
#93124=CARTESIAN_POINT ( 'NONE',  ( -92.55184653144422668, -24.15620529776627734, 10.23563542870659937 ) ) ;
#93126=CARTESIAN_POINT ( 'NONE',  ( -0.9571703918902072505, -22.19477237104690914, 11.49999999999999645 ) ) ;
#93127=EDGE_LOOP ( 'NONE', ( #79916, #4879, #91130, #82378 ) ) ;
#93128=DIRECTION ( 'NONE',  ( 0.000000000000000000, -0.9999999999976377785, -2.173523156925979128E-06 ) ) ;
#93129=CARTESIAN_POINT ( 'NONE',  ( -44.62287095715004881, -23.48786465467240347, 11.44779295918255180 ) ) ;
#93130=ORIENTED_EDGE ( 'NONE', *, *, #18217, .F. ) ;
#93131=CARTESIAN_POINT ( 'NONE',  ( -21.16596634977960179, 8.012090315382277339, -1.500000000000002220 ) ) ;
#93133=EDGE_LOOP ( 'NONE', ( #14604, #20486, #2996, #97118 ) ) ;
#93134=ORIENTED_EDGE ( 'NONE', *, *, #2880, .F. ) ;
#93135=AXIS2_PLACEMENT_3D ( 'NONE', #4469, #42538, #28286 ) ;
#93137=CARTESIAN_POINT ( 'NONE',  ( 14.24339680280927567, 14.23919408161895284, 11.49999999999998934 ) ) ;
#93138=CARTESIAN_POINT ( 'NONE',  ( -81.62287095715002749, -23.73934037231756378, 11.05740245334329153 ) ) ;
#93140=FACE_OUTER_BOUND ( 'NONE', #42853, .T. ) ;
#93141=CARTESIAN_POINT ( 'NONE',  ( -1.374798071107336206, -22.32369649477951512, -1.500000000000002220 ) ) ;
#93142=ORIENTED_EDGE ( 'NONE', *, *, #32601, .T. ) ;
#93145=LINE ( 'NONE', #71334, #3794 ) ;
#93147=CARTESIAN_POINT ( 'NONE',  ( -100.5228709571500616, -25.00182538069145366, 7.747789668545101982 ) ) ;
#93148=FACE_BOUND ( 'NONE', #37013, .T. ) ;
#93149=B_SPLINE_CURVE_WITH_KNOTS ( 'NONE', 3,
 ( #22776, #21780, #84190, #36522, #83695, #67489, #28915, #92306 ),
 .UNSPECIFIED., .F., .F.,
 ( 4, 2, 2, 4 ),
 ( -0.001224873891641431716, -0.0002244903592271139166, 0.0007758931731872038828, 0.002776660238015839482 ),
 .UNSPECIFIED. ) ;
#93150=CARTESIAN_POINT ( 'NONE',  ( 14.87128047407919951, 12.67365258641725312, -1.500000000000002220 ) ) ;
#93151=CARTESIAN_POINT ( 'NONE',  ( -33.58953762381673869, -24.64898659630367206, 1.056161002820377393 ) ) ;
#93152=CARTESIAN_POINT ( 'NONE',  ( 19.88731969966643476, 8.162773808193900749, 11.49999999999998934 ) ) ;
#93153=CARTESIAN_POINT ( 'NONE',  ( -102.5895376238167245, -23.48786465467241769, 11.44779295918253936 ) ) ;
#93155=PLANE ( 'NONE',  #24700 ) ;
#93156=CARTESIAN_POINT ( 'NONE',  ( -111.6228709571500559, -24.51283580621365132, 0.6167428607019819209 ) ) ;
#93157=CARTESIAN_POINT ( 'NONE',  ( -4.526818761702180893, -22.41603498850323817, -1.500000000000002220 ) ) ;
#93158=AXIS2_PLACEMENT_3D ( 'NONE', #19936, #6209, #28065 ) ;
#93160=CARTESIAN_POINT ( 'NONE',  ( -96.52217807345559208, -23.48786465467241413, 11.44779295918254469 ) ) ;
#93161=CARTESIAN_POINT ( 'NONE',  ( -71.18709340149318621, -25.29354215769174985, 5.743106921551899724 ) ) ;
#93162=CARTESIAN_POINT ( 'NONE',  ( -7.547287378330592489, -18.53391252851691462, 11.49999999999999645 ) ) ;
#93163=CARTESIAN_POINT ( 'NONE',  ( -79.55620429048339304, -23.48783264082478794, -1.443836473390066821 ) ) ;
#93164=LINE ( 'NONE', #69849, #24156 ) ;
#93165=EDGE_CURVE ( 'NONE', #30912, #47809, #87434, .T. ) ;
#93166=ADVANCED_FACE ( 'NONE', ( #66185 ), #5250, .F. ) ;
#93167=FACE_OUTER_BOUND ( 'NONE', #44822, .T. ) ;
#93169=ORIENTED_EDGE ( 'NONE', *, *, #1321, .F. ) ;
#93170=DIRECTION ( 'NONE',  ( 0.000000000000000000, -0.9999999999976377785, -2.173523156925979975E-06 ) ) ;
#93171=LINE ( 'NONE', #84566, #97702 ) ;
#93173=EDGE_CURVE ( 'NONE', #60837, #9193, #85098, .T. ) ;
#93174=CARTESIAN_POINT ( 'NONE',  ( -12.31242093702619123, -17.95196869449987531, 11.49999999999998934 ) ) ;
#93175=CARTESIAN_POINT ( 'NONE',  ( -45.52287095715006870, -24.92604778743017491, 8.074972756849357225 ) ) ;
#93176=CARTESIAN_POINT ( 'NONE',  ( 6.681059570357060551, -18.48443787736713873, -1.500000000000002220 ) ) ;
#93177=EDGE_CURVE ( 'NONE', #36980, #36016, #74138, .T. ) ;
#93179=DIRECTION ( 'NONE',  ( -1.000000000000000000, -3.773278334444166432E-23, -8.201307841325785021E-29 ) ) ;
#93181=FACE_OUTER_BOUND ( 'NONE', #7612, .T. ) ;
#93183=CARTESIAN_POINT ( 'NONE',  ( -91.51836248188099887, -23.73791477778912196, 11.05961554403170410 ) ) ;
#93184=LINE ( 'NONE', #85575, #75082 ) ;
#93185=CARTESIAN_POINT ( 'NONE',  ( 6.154377932377651739, 19.64630176443789367, 11.49999999999999645 ) ) ;
#93188=ORIENTED_EDGE ( 'NONE', *, *, #60694, .F. ) ;
#93189=CARTESIAN_POINT ( 'NONE',  ( -80.72727483400176141, -25.26273766163786405, 3.802328419063494280 ) ) ;
#93190=CARTESIAN_POINT ( 'NONE',  ( -26.49029821382958616, -24.85479087585913049, 6.874653004683789703 ) ) ;
#93191=B_SPLINE_CURVE_WITH_KNOTS ( 'NONE', 3,
 ( #61867, #23274, #70471, #8572, #85186, #25286 ),
 .UNSPECIFIED., .F., .F.,
 ( 4, 2, 4 ),
 ( 0.000000000000000000, 0.001380764517853249034, 0.002761529035706498068 ),
 .UNSPECIFIED. ) ;
#93192=CARTESIAN_POINT ( 'NONE',  ( -125.5198022206274686, -24.73531770709095312, 8.716586749053508498 ) ) ;
#93193=DIRECTION ( 'NONE',  ( -3.773278334453079030E-23, 0.9999999999976377785, 2.173523156925979128E-06 ) ) ;
#93194=B_SPLINE_CURVE_WITH_KNOTS ( 'NONE', 3,
 ( #73319, #3814, #81919, #65725 ),
 .UNSPECIFIED., .F., .F.,
 ( 4, 4 ),
 ( 0.2506790037405462468, 0.2596854350126617805 ),
 .UNSPECIFIED. ) ;
#93196=FACE_OUTER_BOUND ( 'NONE', #2669, .T. ) ;
#93197=VERTEX_POINT ( 'NONE', #3771 ) ;
#93198=EDGE_CURVE ( 'NONE', #57335, #42504, #34260, .T. ) ;
#93199=CARTESIAN_POINT ( 'NONE',  ( 8.428894486204411507, 21.44871590506140890, 11.49999999999999645 ) ) ;
#93200=CARTESIAN_POINT ( 'NONE',  ( 19.59772090806136902, -11.66877021596143926, -1.500000000000002220 ) ) ;
#93202=CARTESIAN_POINT ( 'NONE',  ( -67.52287095715011844, -23.96127896941631974, -0.6493128931038022467 ) ) ;
#93203=CARTESIAN_POINT ( 'NONE',  ( -85.55620429048336462, -24.99156044556201905, 7.747789690856173195 ) ) ;
#93205=CARTESIAN_POINT ( 'NONE',  ( 15.48037617655995923, 16.25473645317415361, 11.49999999999999645 ) ) ;
#93207=LINE ( 'NONE', #31313, #81681 ) ;
#93209=CARTESIAN_POINT ( 'NONE',  ( -19.17877449816284496, 10.63638241594707345, 11.49999999999998934 ) ) ;
#93210=CARTESIAN_POINT ( 'NONE',  ( -113.5228709571500474, -23.73907113216990084, -1.053371485793245466 ) ) ;
#93211=CARTESIAN_POINT ( 'NONE',  ( -34.48973961494164087, -24.35071581493542681, 9.817618358456032368 ) ) ;
#93212=CARTESIAN_POINT ( 'NONE',  ( -74.52287095715007581, -23.48786465467241058, 11.44779295918254647 ) ) ;
#93213=VERTEX_POINT ( 'NONE', #19972 ) ;
#93214=CARTESIAN_POINT ( 'NONE',  ( -78.58187477321953907, -24.65952944569304606, 1.056160979905704789 ) ) ;
#93216=ORIENTED_EDGE ( 'NONE', *, *, #75071, .T. ) ;
#93217=CARTESIAN_POINT ( 'NONE',  ( 10.21088607376515789, 17.76353854702842483, 11.49999999999998934 ) ) ;
#93218=ORIENTED_EDGE ( 'NONE', *, *, #97578, .F. ) ;
#93219=ORIENTED_EDGE ( 'NONE', *, *, #95764, .F. ) ;
#93221=ORIENTED_EDGE ( 'NONE', *, *, #5033, .T. ) ;
#93222=CARTESIAN_POINT ( 'NONE',  ( -10.32085834726444595, 20.65377284989807194, -1.500000000000002220 ) ) ;
#93223=CARTESIAN_POINT ( 'NONE',  ( -29.24636659180999843, -25.20264517434234364, 4.940287045316306802 ) ) ;
#93224=CARTESIAN_POINT ( 'NONE',  ( -8.335131950130996614, 18.48905954037022781, -1.500000000000002220 ) ) ;
#93227=CARTESIAN_POINT ( 'NONE',  ( -41.86995616089614458, -25.28979658489737048, 4.210709715701590028 ) ) ;
#93229=CARTESIAN_POINT ( 'NONE',  ( -93.92287095715006728, -23.47596703998600631, 11.44779298504227860 ) ) ;
#93231=CARTESIAN_POINT ( 'NONE',  ( 17.49997855696484095, 12.48231381050728928, 11.49999999999999645 ) ) ;
#93233=CARTESIAN_POINT ( 'NONE',  ( -75.53595366234340247, -24.92564183028979130, 1.928384488918256645 ) ) ;
#93234=CARTESIAN_POINT ( 'NONE',  ( -61.54323830618671565, -24.35071581493542681, 9.817618358456030592 ) ) ;
#93236=B_SPLINE_CURVE_WITH_KNOTS ( 'NONE', 3,
 ( #92485, #23458, #7247, #22956, #47330, #54441, #78253, #70160, #643, #32091, #8766, #55446, #39702, #37707, #70664, #31592, #1155, #86386 ),
 .UNSPECIFIED., .F., .F.,
 ( 4, 2, 2, 2, 2, 2, 2, 2, 4 ),
 ( 0.004711262329854501267, 0.005300117079684243601, 0.005888971829513986803, 0.006477826579343729137, 0.007066681329173471471, 0.007655536079003214672, 0.008244390828832957874, 0.008833245578662701075, 0.009422100328492442542 ),
 .UNSPECIFIED. ) ;
#93237=CARTESIAN_POINT ( 'NONE',  ( 12.91705851660734972, -16.24616318834520001, -1.500000000000002220 ) ) ;
#93238=EDGE_CURVE ( 'NONE', #74917, #93802, #43957, .T. ) ;
#93239=VECTOR ( 'NONE', #25201, 1000.000000000000114 ) ;
#93244=CARTESIAN_POINT ( 'NONE',  ( -75.62287095715004170, -24.62285846362214770, 9.038163152653526211 ) ) ;
#93246=EDGE_LOOP ( 'NONE', ( #57057, #40052, #38892, #74544 ) ) ;
#93247=ORIENTED_EDGE ( 'NONE', *, *, #99352, .T. ) ;
#93249=DIRECTION ( 'NONE',  ( 0.000000000000000000, -0.9999999999976377785, -2.173523156925979128E-06 ) ) ;
#93251=CARTESIAN_POINT ( 'NONE',  ( -76.52287095715006160, -24.35013146730202749, 9.818937971375101270 ) ) ;
#93252=CARTESIAN_POINT ( 'NONE',  ( -14.94409825380703616, 16.19114737329946507, 11.49999999999999645 ) ) ;
#93254=DIRECTION ( 'NONE',  ( -3.773278334453080206E-23, 0.9999999999976377785, 2.173523156925979975E-06 ) ) ;
#93255=CARTESIAN_POINT ( 'NONE',  ( 11.64696156460271581, 19.30390316350253244, 11.49999999999998934 ) ) ;
#93256=CARTESIAN_POINT ( 'NONE',  ( 20.78037738254806399, 3.014218216234254566, -1.500000000000002220 ) ) ;
#93257=CARTESIAN_POINT ( 'NONE',  ( -105.5562042904834072, -23.47593901973091235, -1.443836447538999312 ) ) ;
#93260=DIRECTION ( 'NONE',  ( -0.5473052603529005022, 0.000000000000000000, 0.8369330630283666750 ) ) ;
#93263=CARTESIAN_POINT ( 'NONE',  ( 19.97935793590388442, -6.945280299276400449, -1.500000000000002220 ) ) ;
#93264=DIRECTION ( 'NONE',  ( -1.000000000000000000, -3.773278334444167608E-23, -8.201307833595939069E-29 ) ) ;
#93265=CARTESIAN_POINT ( 'NONE',  ( -51.63614490863932360, -25.26040999518159680, 7.022165695762002890 ) ) ;
#93266=CARTESIAN_POINT ( 'NONE',  ( -121.5532452859548584, -24.65952944569305316, 1.056160979905709008 ) ) ;
#93267=LINE ( 'NONE', #54732, #8713 ) ;
#93269=CARTESIAN_POINT ( 'NONE',  ( -20.56242917251232782, -8.299981740788712870, -1.500000000000002220 ) ) ;
#93270=CARTESIAN_POINT ( 'NONE',  ( -71.50676032721460729, -24.15543982623907127, -0.2315651400026636497 ) ) ;
#93271=ORIENTED_EDGE ( 'NONE', *, *, #51731, .F. ) ;
#93272=CARTESIAN_POINT ( 'NONE',  ( -51.04357394935764347, -25.31633084621363494, 4.940877927261252189 ) ) ;
#93273=CARTESIAN_POINT ( 'NONE',  ( -64.62287095715004170, -23.72773821059535848, 11.05748984161097503 ) ) ;
#93274=CARTESIAN_POINT ( 'NONE',  ( -126.6252818438354240, -23.48783264082477018, -1.443836473390087027 ) ) ;
#93275=CARTESIAN_POINT ( 'NONE',  ( -76.22287095715006444, -23.47593901973090169, -1.443836447538997536 ) ) ;
#93277=CARTESIAN_POINT ( 'NONE',  ( 16.42231304340664266, 10.40281881132301045, 11.49999999999998934 ) ) ;
#93278=AXIS2_PLACEMENT_3D ( 'NONE', #90956, #83839, #36671 ) ;
#93279=CARTESIAN_POINT ( 'NONE',  ( -16.30254408640404051, -13.89340296626662230, 11.49999999999998934 ) ) ;
#93281=CARTESIAN_POINT ( 'NONE',  ( -60.53841807966112043, -24.63419186845290199, 9.035850630957110496 ) ) ;
#93282=CARTESIAN_POINT ( 'NONE',  ( -30.64427850938832165, -23.47593901973090524, -1.443836447538998424 ) ) ;
#93283=CARTESIAN_POINT ( 'NONE',  ( -100.9649361822203133, -25.18440042256897726, 3.436944287541245480 ) ) ;
#93284=CARTESIAN_POINT ( 'NONE',  ( -13.58842472641693711, -18.21064416987719525, -1.500000000000002220 ) ) ;
#93285=CARTESIAN_POINT ( 'NONE',  ( -103.6228709571500985, -23.73907113216991860, -1.053371485793222817 ) ) ;
#93287=CARTESIAN_POINT ( 'NONE',  ( -3.387584560642538101, 19.54024307811383210, 11.49999999999999645 ) ) ;
#93288=CARTESIAN_POINT ( 'NONE',  ( -123.6248514950247852, -24.15620529776629866, 10.23563542870659582 ) ) ;
#93289=EDGE_CURVE ( 'NONE', #72299, #71152, #6395, .T. ) ;
#93293=DIRECTION ( 'NONE',  ( -3.773278334453079030E-23, 0.9999999999976377785, 2.173523156925979128E-06 ) ) ;
#93294=ADVANCED_FACE ( 'NONE', ( #38184 ), #61047, .F. ) ;
#93295=DIRECTION ( 'NONE',  ( -3.773278334444167608E-23, 1.000000000000000000, 0.000000000000000000 ) ) ;
#93296=CARTESIAN_POINT ( 'NONE',  ( -3.891998276399621481, 21.28400606017829233, 11.49999999999998934 ) ) ;
#93297=CARTESIAN_POINT ( 'NONE',  ( -56.62786050513864211, -24.51419770103157347, 9.386484678747180510 ) ) ;
#93298=CARTESIAN_POINT ( 'NONE',  ( 10.09180897563621926, 16.61094848277074476, -1.500000000000002220 ) ) ;
#93300=CARTESIAN_POINT ( 'NONE',  ( -55.54394653881162469, -24.40133493613049964, 9.663955038902800609 ) ) ;
#93303=CARTESIAN_POINT ( 'NONE',  ( 15.88337727998148985, 12.78846505907953279, 11.49999999999999645 ) ) ;
#93304=CARTESIAN_POINT ( 'NONE',  ( -80.59640896514189023, -24.15503026093913164, -0.2815557561904567518 ) ) ;
#93307=LINE ( 'NONE', #31421, #90214 ) ;
#93310=CARTESIAN_POINT ( 'NONE',  ( -62.52287095715006160, -24.64898659630367561, 1.056161002820822592 ) ) ;
#93311=CARTESIAN_POINT ( 'NONE',  ( -48.92504535501358021, -25.31601999834449401, 5.781339443314535309 ) ) ;
#93313=CARTESIAN_POINT ( 'NONE',  ( -34.62287095715005592, -24.66019654487199020, 8.947790411086137041 ) ) ;
#93314=AXIS2_PLACEMENT_3D ( 'NONE', #25780, #63873, #71972 ) ;
#93316=CARTESIAN_POINT ( 'NONE',  ( 8.649182803842551337, -18.14983140373652404, 11.49999999999998934 ) ) ;
#93319=ORIENTED_EDGE ( 'NONE', *, *, #49906, .T. ) ;
#93320=CARTESIAN_POINT ( 'NONE',  ( -81.92287095715006728, -23.47593901973090169, -1.443836447538997092 ) ) ;
#93322=ADVANCED_FACE ( 'NONE', ( #67667 ), #92469, .T. ) ;
#93323=CARTESIAN_POINT ( 'NONE',  ( -11.09240565882118368, -20.00103931635436538, 11.49999999999999645 ) ) ;
#93324=CARTESIAN_POINT ( 'NONE',  ( 17.68435195917723490, -14.24712819257710095, -1.500000000000002220 ) ) ;
#93326=CARTESIAN_POINT ( 'NONE',  ( -80.96226385320385077, -25.14083923594767001, 2.947789366383926968 ) ) ;
#93328=CARTESIAN_POINT ( 'NONE',  ( -38.62372291133213054, -24.66019654487198665, 8.947790411086121054 ) ) ;
#93329=CARTESIAN_POINT ( 'NONE',  ( -30.57287095715006231, -24.76779993212570474, 1.387997001552113696 ) ) ;
#93330=CARTESIAN_POINT ( 'NONE',  ( -84.58953762381673869, -23.48786465467241769, 11.44779295918254469 ) ) ;
#93333=CARTESIAN_POINT ( 'NONE',  ( 8.549789220347504326, 18.50885834720105905, 11.49999999999998934 ) ) ;
#93335=CARTESIAN_POINT ( 'NONE',  ( -21.48638390452810043, -8.140844714011898020, 11.49999999999998934 ) ) ;
#93336=CARTESIAN_POINT ( 'NONE',  ( -54.58737563073252375, -24.35071581493543391, 9.817618358456034144 ) ) ;
#93337=EDGE_LOOP ( 'NONE', ( #4663, #42360, #58298, #51043 ) ) ;
#93338=FACE_OUTER_BOUND ( 'NONE', #48706, .T. ) ;
#93340=B_SPLINE_CURVE_WITH_KNOTS ( 'NONE', 3,
 ( #40249, #71200, #8291, #56494, #93016, #23492 ),
 .UNSPECIFIED., .F., .F.,
 ( 4, 2, 4 ),
 ( 0.000000000000000000, 0.001380764517854765616, 0.002761529035709531232 ),
 .UNSPECIFIED. ) ;
#93342=CARTESIAN_POINT ( 'NONE',  ( 6.245503531335690361, -20.37428601906679759, 11.49999999999999645 ) ) ;
#93344=B_SPLINE_CURVE_WITH_KNOTS ( 'NONE', 3,
 ( #59250, #45031, #29788, #58747 ),
 .UNSPECIFIED., .F., .F.,
 ( 4, 4 ),
 ( 0.000000000000000000, 9.999999999998897304E-05 ),
 .UNSPECIFIED. ) ;
#93345=ORIENTED_EDGE ( 'NONE', *, *, #27260, .F. ) ;
#93346=CARTESIAN_POINT ( 'NONE',  ( 19.10802705166043580, 11.29804532628753044, -1.500000000000002220 ) ) ;
#93347=CARTESIAN_POINT ( 'NONE',  ( 20.28538307770854487, 3.844468116359331944, -1.500000000000002220 ) ) ;
#93348=EDGE_CURVE ( 'NONE', #89111, #95482, #60056, .T. ) ;
#93349=ORIENTED_EDGE ( 'NONE', *, *, #32391, .F. ) ;
#93350=ORIENTED_EDGE ( 'NONE', *, *, #70611, .F. ) ;
#93351=CARTESIAN_POINT ( 'NONE',  ( -108.9567485977555634, -25.27682589219649145, 4.232820627358080401 ) ) ;
#93352=ADVANCED_FACE ( 'NONE', ( #98588 ), #68655, .T. ) ;
#93353=CARTESIAN_POINT ( 'NONE',  ( -95.55787687970359912, -23.85049219812686161, 10.88485053497527133 ) ) ;
#93354=ORIENTED_EDGE ( 'NONE', *, *, #38030, .F. ) ;
#93356=ORIENTED_EDGE ( 'NONE', *, *, #33461, .T. ) ;
#93357=CARTESIAN_POINT ( 'NONE',  ( -58.60466919147697240, -23.73791477778911840, 11.05961554403170766 ) ) ;
#93359=CARTESIAN_POINT ( 'NONE',  ( -19.40898059523135544, 7.551958013340856368, -1.500000000000002220 ) ) ;
#93360=CARTESIAN_POINT ( 'NONE',  ( -1.743439162979827595, 21.76861016152796324, 11.49999999999999645 ) ) ;
#93362=CARTESIAN_POINT ( 'NONE',  ( -27.68651082257923335, -24.89280003935763474, 7.605672334162794535 ) ) ;
#93363=CARTESIAN_POINT ( 'NONE',  ( -78.62985670288350093, -24.35071581493543391, 9.817618358456027039 ) ) ;
#93364=CARTESIAN_POINT ( 'NONE',  ( 16.82713599508461400, -14.87465808564757808, -1.500000000000002220 ) ) ;
#93367=LINE ( 'NONE', #86764, #97144 ) ;
#93369=VERTEX_POINT ( 'NONE', #76733 ) ;
#93373=VECTOR ( 'NONE', #46251, 1000.000000000000227 ) ;
#93374=CARTESIAN_POINT ( 'NONE',  ( 3.515848477382193416, 21.04717058667041130, -1.500000000000002220 ) ) ;
#93375=ORIENTED_EDGE ( 'NONE', *, *, #33658, .F. ) ;
#93377=CARTESIAN_POINT ( 'NONE',  ( -19.68365937621761219, -7.520201837432793468, -1.500000000000002220 ) ) ;
#93378=CARTESIAN_POINT ( 'NONE',  ( -30.58829557286704315, -23.48329323021739512, -1.443836490256471983 ) ) ;
#93379=CARTESIAN_POINT ( 'NONE',  ( -4.495603250223349612, -19.44740727768710187, -1.500000000000002220 ) ) ;
#93380=CARTESIAN_POINT ( 'NONE',  ( -50.57926052499865222, -24.83644354573578283, 8.397322867130100121 ) ) ;
#93381=AXIS2_PLACEMENT_3D ( 'NONE', #19481, #50444, #81391 ) ;
#93383=CARTESIAN_POINT ( 'NONE',  ( -0.4018715335629812202, -22.01094342083549193, -1.500000000000002220 ) ) ;
#93385=ORIENTED_EDGE ( 'NONE', *, *, #98271, .F. ) ;
#93386=B_SPLINE_CURVE_WITH_KNOTS ( 'NONE', 3,
 ( #73398, #19091, #3893, #42953, #34832, #73889 ),
 .UNSPECIFIED., .F., .F.,
 ( 4, 2, 4 ),
 ( 0.000000000000000000, 0.001380901958385385075, 0.002761803916770770150 ),
 .UNSPECIFIED. ) ;
#93387=CARTESIAN_POINT ( 'NONE',  ( -90.62287095715004170, -25.00158670708908915, 2.256160236439166411 ) ) ;
#93389=CARTESIAN_POINT ( 'NONE',  ( 16.93201058511109380, 12.15574511561022852, 11.49999999999999645 ) ) ;
#93392=CARTESIAN_POINT ( 'NONE',  ( -39.62287095715005592, -29.50250243563736774, 8.947779886222148704 ) ) ;
#93393=CARTESIAN_POINT ( 'NONE',  ( -48.62287095715004881, -23.47593901973091235, -1.443836447539009749 ) ) ;
#93394=CARTESIAN_POINT ( 'NONE',  ( -19.99249555334884221, 7.427959064407942513, -1.500000000000002220 ) ) ;
#93395=CARTESIAN_POINT ( 'NONE',  ( -31.24388727629348494, -24.86441894802673147, 8.247789967202360017 ) ) ;
#93396=CARTESIAN_POINT ( 'NONE',  ( -124.5228709571500616, -24.50216790748203977, 0.6166512839542644953 ) ) ;
#93397=CARTESIAN_POINT ( 'NONE',  ( -90.62287095715001328, -24.14321612903114556, -0.2833117244521682343 ) ) ;
#93399=CARTESIAN_POINT ( 'NONE',  ( 22.09666729679958053, 4.251135690456572469, -1.500000000000002220 ) ) ;
#93400=CARTESIAN_POINT ( 'NONE',  ( -108.8763703466142800, -25.32390614315827193, 4.358500768180118889 ) ) ;
#93402=DIRECTION ( 'NONE',  ( -3.773278334453079030E-23, 0.9999999999976377785, 2.173523156925979128E-06 ) ) ;
#93404=CARTESIAN_POINT ( 'NONE',  ( -6.756748142665309764, -18.51622224137248907, 11.49999999999999645 ) ) ;
#93406=B_SPLINE_CURVE_WITH_KNOTS ( 'NONE', 3,
 ( #80108, #48175, #1998, #87220, #40055, #9601 ),
 .UNSPECIFIED., .F., .F.,
 ( 4, 2, 4 ),
 ( 6.384118678613675148E-06, 0.001386860460828376936, 0.002767336802978140158 ),
 .UNSPECIFIED. ) ;
#93408=EDGE_LOOP ( 'NONE', ( #37359, #54963, #41317, #45155 ) ) ;
#93410=CARTESIAN_POINT ( 'NONE',  ( -108.5562042904833930, -24.66019654487199730, 8.947790411086121054 ) ) ;
#93411=CARTESIAN_POINT ( 'NONE',  ( -88.87354082327544802, -25.06732983082694588, 7.447789526168958396 ) ) ;
#93414=CARTESIAN_POINT ( 'NONE',  ( 17.05426814964238957, 9.943002105365778220, 11.49999999999998934 ) ) ;
#93415=ORIENTED_EDGE ( 'NONE', *, *, #52435, .T. ) ;
#93419=B_SPLINE_CURVE_WITH_KNOTS ( 'NONE', 3,
 ( #16147, #86164, #1441, #46617 ),
 .UNSPECIFIED., .F., .F.,
 ( 4, 4 ),
 ( 0.000000000000000000, 0.0001000000000000028644 ),
 .UNSPECIFIED. ) ;
#93423=DIRECTION ( 'NONE',  ( -3.773278334453079030E-23, 0.9999999999976377785, 2.173523156925979128E-06 ) ) ;
#93425=CARTESIAN_POINT ( 'NONE',  ( -99.83839741074528717, -25.26638519438374075, 7.461409190821002291 ) ) ;
#93426=PLANE ( 'NONE',  #35549 ) ;
#93428=CARTESIAN_POINT ( 'NONE',  ( -53.52287095715006870, -24.65952944569304606, 1.056160979905693686 ) ) ;
#93429=CARTESIAN_POINT ( 'NONE',  ( -13.93161493328335432, -14.37010051631055418, -1.500000000000002220 ) ) ;
#93430=EDGE_CURVE ( 'NONE', #31349, #78091, #24527, .T. ) ;
#93431=CARTESIAN_POINT ( 'NONE',  ( -99.12380231474227799, -25.10935291788973345, 4.001575492514970911 ) ) ;
#93436=CARTESIAN_POINT ( 'NONE',  ( -109.7896840091628832, -25.18430186498734358, 3.444318112836231904 ) ) ;
#93437=CARTESIAN_POINT ( 'NONE',  ( -58.52287095715004739, -23.73934037231756022, 11.05740245334328797 ) ) ;
#93438=CARTESIAN_POINT ( 'NONE',  ( -100.6228709571500559, -23.48786465467241769, 11.44779295918254114 ) ) ;
#93440=CARTESIAN_POINT ( 'NONE',  ( -51.70072539166533687, -25.31574255575237231, 3.987151966999201491 ) ) ;
#93441=VECTOR ( 'NONE', #73389, 1000.000000000000114 ) ;
#93442=FACE_OUTER_BOUND ( 'NONE', #5152, .T. ) ;
#93443=DIRECTION ( 'NONE',  ( 0.000000000000000000, 0.9999999999976377785, 2.173523156925979975E-06 ) ) ;
#93446=AXIS2_PLACEMENT_3D ( 'NONE', #65218, #65711, #50463 ) ;
#93447=CARTESIAN_POINT ( 'NONE',  ( 19.35245777310151993, -6.127589836641541332, -1.500000000000002220 ) ) ;
#93448=DIRECTION ( 'NONE',  ( -0.5644074343637431879, 0.000000000000000000, 0.8254963646406547895 ) ) ;
#93450=DIRECTION ( 'NONE',  ( -3.773278334453079618E-23, 0.9999999999976377785, 2.173523156925979975E-06 ) ) ;
#93451=ORIENTED_EDGE ( 'NONE', *, *, #6344, .F. ) ;
#93452=CARTESIAN_POINT ( 'NONE',  ( -113.5228709571500616, -29.50250243563736774, 8.947779886222136270 ) ) ;
#93454=CARTESIAN_POINT ( 'NONE',  ( -19.30929855918770954, 5.666966705251045511, -1.500000000000002220 ) ) ;
#93455=CARTESIAN_POINT ( 'NONE',  ( -15.55823947972799282, -14.28038451723262270, 11.49999999999999645 ) ) ;
#93456=CARTESIAN_POINT ( 'NONE',  ( -16.97254739485517661, -14.18817111035334655, -1.500000000000002220 ) ) ;
#93457=EDGE_CURVE ( 'NONE', #81901, #46658, #99638, .T. ) ;
#93458=CARTESIAN_POINT ( 'NONE',  ( -18.11865614447288664, 9.752654332028551920, -1.500000000000002220 ) ) ;
#93459=CARTESIAN_POINT ( 'NONE',  ( -60.63096549711488592, -24.73486907724917572, 1.287355809206962798 ) ) ;
#93462=ORIENTED_EDGE ( 'NONE', *, *, #87942, .F. ) ;
#93465=ORIENTED_EDGE ( 'NONE', *, *, #12771, .T. ) ;
#93468=CARTESIAN_POINT ( 'NONE',  ( -53.62287095715005592, -29.50248528299804818, 1.056150453629033370 ) ) ;
#93469=CARTESIAN_POINT ( 'NONE',  ( -63.62287095715004881, -24.51283580621364067, 0.6167428607019798115 ) ) ;
#93471=CARTESIAN_POINT ( 'NONE',  ( -18.80638259998596951, 8.471300643254643603, -1.500000000000002220 ) ) ;
#93472=CARTESIAN_POINT ( 'NONE',  ( 21.54666897473465070, 1.519730039111064412, 11.49999999999999645 ) ) ;
#93477=CARTESIAN_POINT ( 'NONE',  ( -22.26391555059773353, 2.265117081278330780, 11.49999999999998934 ) ) ;
#93478=CARTESIAN_POINT ( 'NONE',  ( -71.52287095715007581, -24.65952944569304606, 1.056160979905697239 ) ) ;
#93479=CARTESIAN_POINT ( 'NONE',  ( -120.6228709571500559, -24.14406661707769786, 10.28769366152061160 ) ) ;
#93482=CARTESIAN_POINT ( 'NONE',  ( -108.5228709571500616, -29.50248528299804818, 1.056150453629043584 ) ) ;
#93484=CARTESIAN_POINT ( 'NONE',  ( -11.35812032211249090, 17.58211214940072864, -1.500000000000002220 ) ) ;
#93485=ORIENTED_EDGE ( 'NONE', *, *, #25488, .F. ) ;
#93491=CARTESIAN_POINT ( 'NONE',  ( -128.6228709571500417, -24.64965695001469115, 8.947790433994173398 ) ) ;
#93492=CARTESIAN_POINT ( 'NONE',  ( 3.428800225705347149, -20.88102749682517612, -1.500000000000002220 ) ) ;
#93494=CARTESIAN_POINT ( 'NONE',  ( -89.62287095715004170, -29.50247984919015209, -1.443849546365051806 ) ) ;
#93495=CARTESIAN_POINT ( 'NONE',  ( -21.66901994843296819, -2.608494568651300138, 11.49999999999998934 ) ) ;
#93498=CARTESIAN_POINT ( 'NONE',  ( -110.6228709571500701, -23.48783264082479505, -1.443836473390060160 ) ) ;
#93499=CARTESIAN_POINT ( 'NONE',  ( 20.45693200876408469, 7.529271608661172621, -1.500000000000002220 ) ) ;
#93501=ORIENTED_EDGE ( 'NONE', *, *, #81843, .F. ) ;
#93504=ORIENTED_EDGE ( 'NONE', *, *, #78480, .T. ) ;
#93505=ADVANCED_FACE ( 'NONE', ( #48321 ), #63054, .F. ) ;
#93507=VERTEX_POINT ( 'NONE', #18362 ) ;
#93509=CARTESIAN_POINT ( 'NONE',  ( -58.52287095715006160, -24.64965694238407323, 8.947790433994201820 ) ) ;
#93511=CARTESIAN_POINT ( 'NONE',  ( 12.26186175617451113, -17.30295086655154080, -1.500000000000002220 ) ) ;
#93512=CARTESIAN_POINT ( 'NONE',  ( -94.62561019970178222, -24.51314013834315375, 0.6176544820404151759 ) ) ;
#93513=FACE_BOUND ( 'NONE', #21856, .T. ) ;
#93516=CARTESIAN_POINT ( 'NONE',  ( 7.305494252837257285, 17.95555029072639286, 11.49999999999998934 ) ) ;
#93517=CARTESIAN_POINT ( 'NONE',  ( -41.88795169677845109, -25.25978494880519776, 3.590542803917028181 ) ) ;
#93518=ORIENTED_EDGE ( 'NONE', *, *, #99013, .F. ) ;
#93519=CARTESIAN_POINT ( 'NONE',  ( 10.22484414329051994, 16.58839404647166660, 11.49999999999999645 ) ) ;
#93523=CARTESIAN_POINT ( 'NONE',  ( -80.33862689906705157, -25.12417942247672542, 7.094867700071801231 ) ) ;
#93526=CARTESIAN_POINT ( 'NONE',  ( -97.62287095715005592, -29.50250786944525672, 11.44777988621623166 ) ) ;
#93527=CARTESIAN_POINT ( 'NONE',  ( -30.50620355600309708, -23.47593905652042778, -1.426910232161149983 ) ) ;
#93528=CARTESIAN_POINT ( 'NONE',  ( -93.59138280458586223, -24.15620529776628445, 10.23563542870659404 ) ) ;
#93529=CARTESIAN_POINT ( 'NONE',  ( -6.620539020842763911, -18.51205181221761720, -1.500000000000002220 ) ) ;
#93530=CARTESIAN_POINT ( 'NONE',  ( -41.46611000704998418, -25.27805945495849826, 4.188173683520152402 ) ) ;
#93532=CARTESIAN_POINT ( 'NONE',  ( 21.36531308999010648, 3.172564587314818052, -1.500000000000002220 ) ) ;
#93533=CARTESIAN_POINT ( 'NONE',  ( -40.57216908292625845, -25.00158670708910336, 2.256160236439222366 ) ) ;
#93534=PLANE ( 'NONE',  #55289 ) ;
#93535=CARTESIAN_POINT ( 'NONE',  ( -22.28253579152010033, 6.022996098971622914, -1.500000000000002220 ) ) ;
#93538=CARTESIAN_POINT ( 'NONE',  ( -57.52287095715005449, -29.50248528299804818, 1.056150453629034924 ) ) ;
#93539=CARTESIAN_POINT ( 'NONE',  ( -49.62287095715005592, -29.50250786944525672, 11.44777988621624054 ) ) ;
#93540=LINE ( 'NONE', #207, #21741 ) ;
#93542=CARTESIAN_POINT ( 'NONE',  ( -110.2102236481481015, -25.18562194707735813, 3.298800634353756589 ) ) ;
#93543=CARTESIAN_POINT ( 'NONE',  ( -129.5221661632653536, -23.73766607897671221, -1.055555164236443577 ) ) ;
#93544=CARTESIAN_POINT ( 'NONE',  ( -111.3738206124644279, -25.29779372368820134, 4.292346609405336189 ) ) ;
#93545=CARTESIAN_POINT ( 'NONE',  ( -13.91458393394894166, 14.26456941660895339, 11.49999999999998934 ) ) ;
#93546=EDGE_CURVE ( 'NONE', #15184, #42104, #5120, .T. ) ;
#93547=CARTESIAN_POINT ( 'NONE',  ( -69.52287095715006160, -23.47593901973090169, -1.443836447538996870 ) ) ;
#93548=CARTESIAN_POINT ( 'NONE',  ( -11.71124675921804403, 15.99993322257668282, -1.500000000000002220 ) ) ;
#93551=B_SPLINE_CURVE_WITH_KNOTS ( 'NONE', 3,
 ( #79544, #50111, #81049, #19638 ),
 .UNSPECIFIED., .F., .F.,
 ( 4, 4 ),
 ( 0.000000000000000000, 0.0001000000000000167422 ),
 .UNSPECIFIED. ) ;
#93552=CARTESIAN_POINT ( 'NONE',  ( -40.25203966287474344, -25.29116520055095663, 2.839406929231615528 ) ) ;
#93553=CARTESIAN_POINT ( 'NONE',  ( -35.62287095715005592, -23.47596703998600276, 11.44779298504227505 ) ) ;
#93554=CARTESIAN_POINT ( 'NONE',  ( -19.90621922972506397, 5.769413876575915978, 11.49999999999999645 ) ) ;
#93557=CARTESIAN_POINT ( 'NONE',  ( -88.62287095715007013, -23.94994826722515668, -0.6494450866351709761 ) ) ;
#93558=CARTESIAN_POINT ( 'NONE',  ( -6.081610112697643622, 21.96313418072945822, 11.49999999999999645 ) ) ;
#93559=ORIENTED_EDGE ( 'NONE', *, *, #34440, .F. ) ;
#93560=B_SPLINE_SURFACE_WITH_KNOTS ( 'NONE', 3, 3, ( 
 ( #32946, #26822, #65420, #11589 ),
 ( #33940, #88233, #33435, #87731 ),
 ( #49186, #88732, #50171, #73012 ),
 ( #55797, #24817, #48176, #94833 ),
 ( #25825, #79104, #81108, #57302 ),
 ( #18697, #64919, #86720, #79608 ),
 ( #96334, #42067, #40562, #3499 ),
 ( #25323, #95833, #72016, #10596 ),
 ( #41563, #56798, #26328, #80109 ),
 ( #49679, #64421, #71515, #80607 ) ),
 .UNSPECIFIED., .F., .F., .F.,
 ( 4, 3, 3, 4 ),
 ( 4, 4 ),
 ( 0.0004766839783818981654, 0.1491231665100171688, 0.2234464077758347988, 0.2977696490416524289 ),
 ( 0.3995422531334771321, 0.4007930632633419643 ),
 .UNSPECIFIED. ) ;
#93561=LINE ( 'NONE', #24055, #5791 ) ;
#93562=CARTESIAN_POINT ( 'NONE',  ( -74.62287095715005592, -23.48786465467241058, 11.44779295918254469 ) ) ;
#93563=VERTEX_POINT ( 'NONE', #71156 ) ;
#93564=CARTESIAN_POINT ( 'NONE',  ( -19.95319933381289701, -3.276446921841525306, 11.49999999999998934 ) ) ;
#93566=CARTESIAN_POINT ( 'NONE',  ( -110.5228709571500616, -23.85229601348997264, 10.88205029486208630 ) ) ;
#93569=VERTEX_POINT ( 'NONE', #79249 ) ;
#93571=CARTESIAN_POINT ( 'NONE',  ( -21.13427563780003382, 8.902639844219676135, -1.500000000000002220 ) ) ;
#93572=CARTESIAN_POINT ( 'NONE',  ( -51.29636648399702636, -25.18439796746319814, 3.969959851941196938 ) ) ;
#93573=CARTESIAN_POINT ( 'NONE',  ( 11.61936018155104833, -18.21891831228114356, -1.500000000000002220 ) ) ;
#93574=CARTESIAN_POINT ( 'NONE',  ( -104.6228709571500559, -23.48783264082478794, -1.443836473390062158 ) ) ;
#93575=CARTESIAN_POINT ( 'NONE',  ( -20.02981537788295441, -6.213780249082809348, 11.49999999999999645 ) ) ;
#93576=ORIENTED_EDGE ( 'NONE', *, *, #44028, .T. ) ;
#93577=LINE ( 'NONE', #59795, #82583 ) ;
#93578=CARTESIAN_POINT ( 'NONE',  ( -68.94044447473358161, -25.24754525613202460, 6.138838922787388519 ) ) ;
#93579=CARTESIAN_POINT ( 'NONE',  ( -1.213202359833694732, 22.00568734548514627, -1.500000000000002220 ) ) ;
#93581=CARTESIAN_POINT ( 'NONE',  ( -98.52287095715006160, -24.64965694238575011, 8.947790433994194714 ) ) ;
#93582=CARTESIAN_POINT ( 'NONE',  ( -66.55620429048337883, -24.64965694238574656, 8.947790433994198267 ) ) ;
#93583=EDGE_CURVE ( 'NONE', #53349, #13741, #92285, .T. ) ;
#93584=ORIENTED_EDGE ( 'NONE', *, *, #13147, .T. ) ;
#93586=CARTESIAN_POINT ( 'NONE',  ( -122.6228709571500417, -24.50321055353805377, 9.387540953477525818 ) ) ;
#93587=ORIENTED_EDGE ( 'NONE', *, *, #94892, .T. ) ;
#93590=VECTOR ( 'NONE', #25396, 1000.000000000000227 ) ;
#93591=ORIENTED_EDGE ( 'NONE', *, *, #69966, .F. ) ;
#93593=CARTESIAN_POINT ( 'NONE',  ( -95.62287095715002749, -25.00182538069145721, 7.747789668545097541 ) ) ;
#93594=CARTESIAN_POINT ( 'NONE',  ( -36.52733198375308632, -24.65952944569304606, 1.056160979905694353 ) ) ;
#93595=CARTESIAN_POINT ( 'NONE',  ( 16.11427877760282001, 12.65940972936023812, -1.500000000000002220 ) ) ;
#93596=ORIENTED_EDGE ( 'NONE', *, *, #22103, .T. ) ;
#93597=CARTESIAN_POINT ( 'NONE',  ( -99.83650425372744053, -25.30067960901012825, 5.350007036700404228 ) ) ;
#93598=CARTESIAN_POINT ( 'NONE',  ( -44.49966819881763769, -24.15543982623906771, -0.2315651400026670914 ) ) ;
#93600=CARTESIAN_POINT ( 'NONE',  ( 22.08996893241407378, 3.065900275835479860, -1.500000000000002220 ) ) ;
#93601=CARTESIAN_POINT ( 'NONE',  ( -70.56836343276164314, -25.13731425188323954, 7.077682618907291889 ) ) ;
#93602=CARTESIAN_POINT ( 'NONE',  ( -27.33175959122838350, -24.62075588168795903, 8.217702253644940669 ) ) ;
#93603=ORIENTED_EDGE ( 'NONE', *, *, #44413, .F. ) ;
#93604=CARTESIAN_POINT ( 'NONE',  ( -28.17037414371105086, -24.65651949530377962, 1.683498270968381005 ) ) ;
#93606=CARTESIAN_POINT ( 'NONE',  ( -14.80784184970232431, -14.63167926507950689, 11.49999999999998934 ) ) ;
#93607=EDGE_LOOP ( 'NONE', ( #32028, #69932, #88533, #86452 ) ) ;
#93608=B_SPLINE_CURVE_WITH_KNOTS ( 'NONE', 3,
 ( #47861, #1182, #8791, #94020 ),
 .UNSPECIFIED., .F., .F.,
 ( 4, 4 ),
 ( 0.8904217528559288386, 0.8994281841280442613 ),
 .UNSPECIFIED. ) ;
#93609=CARTESIAN_POINT ( 'NONE',  ( -51.58953762381672448, -24.64898659630367206, 1.056161002820380279 ) ) ;
#93610=ORIENTED_EDGE ( 'NONE', *, *, #83449, .F. ) ;
#93611=EDGE_CURVE ( 'NONE', #21327, #98355, #94811, .T. ) ;
#93613=CARTESIAN_POINT ( 'NONE',  ( -51.38881019666819583, -25.12217764763901329, 6.651362562939564071 ) ) ;
#93614=CARTESIAN_POINT ( 'NONE',  ( 19.96068868648078620, -6.529529906025321573, -1.500000000000002220 ) ) ;
#93615=EDGE_CURVE ( 'NONE', #72949, #42580, #14812, .T. ) ;
#93616=VERTEX_POINT ( 'NONE', #31578 ) ;
#93617=CARTESIAN_POINT ( 'NONE',  ( -110.6228709571500985, -24.62226745350443124, 0.9660975649729638404 ) ) ;
#93621=CARTESIAN_POINT ( 'NONE',  ( -59.53434381846648904, -24.65952944569304961, 1.056160979905697905 ) ) ;
#93622=CARTESIAN_POINT ( 'NONE',  ( -57.52287095715004739, -23.73907113216988307, -1.053371485793252571 ) ) ;
#93623=CARTESIAN_POINT ( 'NONE',  ( -19.97062832128981213, -9.750827054148329509, 11.49999999999999645 ) ) ;
#93625=CARTESIAN_POINT ( 'NONE',  ( -98.93782592301593581, -25.29244077744215247, 5.755742261006358440 ) ) ;
#93626=DIRECTION ( 'NONE',  ( 3.773278334444167608E-23, -1.000000000000000000, 0.000000000000000000 ) ) ;
#93627=EDGE_LOOP ( 'NONE', ( #6091, #5499, #15403, #2167 ) ) ;
#93628=CARTESIAN_POINT ( 'NONE',  ( -18.33335541821337245, -13.34141728429830742, -1.500000000000002220 ) ) ;
#93629=AXIS2_PLACEMENT_3D ( 'NONE', #12028, #4926, #52098 ) ;
#93630=ADVANCED_FACE ( 'NONE', ( #86372 ), #47316, .T. ) ;
#93632=DIRECTION ( 'NONE',  ( -3.773278334453080206E-23, 0.9999999999976377785, 2.173523156925979975E-06 ) ) ;
#93633=ORIENTED_EDGE ( 'NONE', *, *, #65723, .F. ) ;
#93634=EDGE_LOOP ( 'NONE', ( #29953, #94077, #19492, #35235 ) ) ;
#93635=EDGE_CURVE ( 'NONE', #49044, #65549, #30649, .T. ) ;
#93637=CARTESIAN_POINT ( 'NONE',  ( -10.68008619461380704, -17.10268970254769982, -1.500000000000002220 ) ) ;
#93638=CARTESIAN_POINT ( 'NONE',  ( -80.62287095715005592, -23.85196035786901092, -0.8779234886474913679 ) ) ;
#93639=ORIENTED_EDGE ( 'NONE', *, *, #52810, .T. ) ;
#93640=CARTESIAN_POINT ( 'NONE',  ( -108.6228709571500417, -23.47596703998600631, 11.44779298504227860 ) ) ;
#93641=CARTESIAN_POINT ( 'NONE',  ( 14.42577177192597482, -17.14957960503723911, -1.500000000000002220 ) ) ;
#93642=EDGE_CURVE ( 'NONE', #47809, #81499, #89956, .T. ) ;
#93643=B_SPLINE_CURVE_WITH_KNOTS ( 'NONE', 3,
 ( #44542, #75466, #5970, #6476, #53661, #67888 ),
 .UNSPECIFIED., .F., .F.,
 ( 4, 2, 4 ),
 ( 1.570755371634092017E-05, 0.001396183895866087970, 0.002776660238015834711 ),
 .UNSPECIFIED. ) ;
#93644=ORIENTED_EDGE ( 'NONE', *, *, #77702, .T. ) ;
#93647=CARTESIAN_POINT ( 'NONE',  ( -119.6228709571500559, -23.72773821059535493, 11.05748984161097503 ) ) ;
#93648=CARTESIAN_POINT ( 'NONE',  ( -39.47555198290115186, -25.30229325268190976, 4.430735662431675159 ) ) ;
#93650=VECTOR ( 'NONE', #28279, 1000.000000000000114 ) ;
#93651=B_SPLINE_CURVE_WITH_KNOTS ( 'NONE', 3,
 ( #60508, #52881, #83820, #16809, #32539, #77688 ),
 .UNSPECIFIED., .F., .F.,
 ( 4, 2, 4 ),
 ( 1.570755371633875854E-05, 0.001396183895866086235, 0.002776660238015833410 ),
 .UNSPECIFIED. ) ;
#93652=CARTESIAN_POINT ( 'NONE',  ( -97.25033046169170348, -24.47827083238275847, 0.5637492489085987879 ) ) ;
#93653=CARTESIAN_POINT ( 'NONE',  ( -9.112395119859147741, -17.30902560603237106, -1.500000000000002220 ) ) ;
#93655=ORIENTED_EDGE ( 'NONE', *, *, #1196, .T. ) ;
#93656=CARTESIAN_POINT ( 'NONE',  ( 15.57385778016992894, -14.83193121981731544, -1.500000000000002220 ) ) ;
#93657=CARTESIAN_POINT ( 'NONE',  ( -62.52287095715010423, -24.35013146730203815, 9.818937971375104823 ) ) ;
#93661=CARTESIAN_POINT ( 'NONE',  ( 7.824713763024562674, 21.46283361357968289, -1.500000000000002220 ) ) ;
#93662=ADVANCED_FACE ( 'NONE', ( #74150 ), #66569, .T. ) ;
#93666=CARTESIAN_POINT ( 'NONE',  ( -101.5562042904833930, -23.47593901973091235, -1.443836447539001089 ) ) ;
#93668=CARTESIAN_POINT ( 'NONE',  ( -15.86121933104946535, 12.22609501325904624, 11.49999999999999645 ) ) ;
#93669=CARTESIAN_POINT ( 'NONE',  ( -79.67189865184847974, -25.31594350486923872, 4.664461505014560139 ) ) ;
#93674=EDGE_LOOP ( 'NONE', ( #61334, #88918, #53804, #95756 ) ) ;
#93675=DIRECTION ( 'NONE',  ( 0.000000000000000000, -2.173523156925980399E-06, 0.9999999999976378895 ) ) ;
#93677=CARTESIAN_POINT ( 'NONE',  ( -20.93004649427559016, -6.003493321846349318, 11.49999999999998934 ) ) ;
#93678=CARTESIAN_POINT ( 'NONE',  ( -56.62287095715004881, -24.66019654487199020, 8.947790411086131712 ) ) ;
#93679=CARTESIAN_POINT ( 'NONE',  ( 8.085132396474181249, 17.94908993440701295, -1.500000000000002220 ) ) ;
#93680=CARTESIAN_POINT ( 'NONE',  ( -124.6228709571500559, -29.50248528299804818, 1.056150453629045360 ) ) ;
#93681=EDGE_CURVE ( 'NONE', #16362, #42205, #80250, .T. ) ;
#93683=CARTESIAN_POINT ( 'NONE',  ( -40.58380419742159262, -25.18557147773197968, 3.298448857756749231 ) ) ;
#93686=CARTESIAN_POINT ( 'NONE',  ( -73.62287095715007013, -23.96177878511307568, 10.65340807706329862 ) ) ;
#93687=CARTESIAN_POINT ( 'NONE',  ( 18.81462172601333549, -8.267562025728075525, 11.49999999999999645 ) ) ;
#93690=CARTESIAN_POINT ( 'NONE',  ( -15.94491270116497184, -16.04792668696150315, 11.49999999999999645 ) ) ;
#93692=FACE_OUTER_BOUND ( 'NONE', #50056, .T. ) ;
#93693=CARTESIAN_POINT ( 'NONE',  ( -37.52287095715006870, -24.50216790748204687, 0.6166512839542470648 ) ) ;
#93694=CARTESIAN_POINT ( 'NONE',  ( -125.5892681715929342, -24.73531770709095312, 8.716586749053508498 ) ) ;
#93695=B_SPLINE_CURVE_WITH_KNOTS ( 'NONE', 3,
 ( #48139, #84680, #1461, #69462 ),
 .UNSPECIFIED., .F., .F.,
 ( 4, 4 ),
 ( 0.3107218788879825278, 0.3197283101600981170 ),
 .UNSPECIFIED. ) ;
#93696=CARTESIAN_POINT ( 'NONE',  ( -85.62287095715001328, -24.92579138211019796, 1.929029949965662460 ) ) ;
#93697=CARTESIAN_POINT ( 'NONE',  ( -25.54628175542703161, -24.93063037130169235, 5.501430938224779688 ) ) ;
#93699=ORIENTED_EDGE ( 'NONE', *, *, #11498, .T. ) ;
#93700=CARTESIAN_POINT ( 'NONE',  ( -79.38647268321243189, -25.26750025236339070, 5.652477768429786664 ) ) ;
#93701=CARTESIAN_POINT ( 'NONE',  ( 7.682656365740156090, -21.48159684637525046, 11.49999999999998934 ) ) ;
#93703=B_SPLINE_SURFACE_WITH_KNOTS ( 'NONE', 3, 3, ( 
 ( #8036, #86661, #24754, #92764 ),
 ( #86163, #16644, #32886, #34755 ),
 ( #16146, #32378, #71454, #70445 ),
 ( #424, #39991, #46615, #77537 ),
 ( #62340, #80928, #19021, #9038 ),
 ( #15647, #78534, #85158, #93772 ),
 ( #63354, #31376, #93266, #47117 ) ),
 .UNSPECIFIED., .F., .F., .F.,
 ( 4, 3, 4 ),
 ( 4, 4 ),
 ( 0.0004766839783822478748, 0.1029713700210899419, 0.2054660560637976419 ),
 ( 0.08951676878467576537, 0.09057079621334723774 ),
 .UNSPECIFIED. ) ;
#93704=CARTESIAN_POINT ( 'NONE',  ( -96.50858727277388027, -24.51314013834316086, 0.6176544820404197278 ) ) ;
#93705=CARTESIAN_POINT ( 'NONE',  ( -86.52287095715003318, -24.33927499327855770, 9.819080762295811837 ) ) ;
#93706=CARTESIAN_POINT ( 'NONE',  ( 6.968497804723354783, -21.30229754059623559, 11.49999999999999645 ) ) ;
#93707=ORIENTED_EDGE ( 'NONE', *, *, #25474, .T. ) ;
#93708=CARTESIAN_POINT ( 'NONE',  ( -70.62287095715005592, -23.85229601348997264, 10.88205029486207920 ) ) ;
#93709=CARTESIAN_POINT ( 'NONE',  ( -3.149188516569510377, 21.71089317892358395, -1.500000000000002220 ) ) ;
#93710=B_SPLINE_CURVE_WITH_KNOTS ( 'NONE', 3,
 ( #17874, #26495, #2664, #34607 ),
 .UNSPECIFIED., .F., .F.,
 ( 4, 4 ),
 ( 0.7210148590621303644, 0.7300212903342458981 ),
 .UNSPECIFIED. ) ;
#93712=CARTESIAN_POINT ( 'NONE',  ( -44.48765446362095588, -24.51419770103159479, 9.386484678747171628 ) ) ;
#93713=CARTESIAN_POINT ( 'NONE',  ( -74.58953762381673869, -23.48786465467241058, 11.44779295918254469 ) ) ;
#93717=ORIENTED_EDGE ( 'NONE', *, *, #65280, .T. ) ;
#93718=CARTESIAN_POINT ( 'NONE',  ( -7.302954156136775232, -19.11528491071161540, 11.49999999999998934 ) ) ;
#93720=VERTEX_POINT ( 'NONE', #3650 ) ;
#93722=ORIENTED_EDGE ( 'NONE', *, *, #32659, .T. ) ;
#93723=CARTESIAN_POINT ( 'NONE',  ( 5.395019145045520048, -22.42585393411717121, 11.49999999999998934 ) ) ;
#93724=CARTESIAN_POINT ( 'NONE',  ( -94.52287095715006160, -29.50250243563736774, 8.947779886222139822 ) ) ;
#93725=CARTESIAN_POINT ( 'NONE',  ( 5.353267490507026771, -19.58905154090721368, -1.500000000000002220 ) ) ;
#93729=CARTESIAN_POINT ( 'NONE',  ( -92.64086922289898496, -23.48783264082478084, -1.443836473390064157 ) ) ;
#93730=DIRECTION ( 'NONE',  ( 0.000000000000000000, 0.9999999999976377785, 2.173523156925979128E-06 ) ) ;
#93732=CARTESIAN_POINT ( 'NONE',  ( 21.49998558720804809, 0.1351929536555107336, 11.49999999999999645 ) ) ;
#93733=ORIENTED_EDGE ( 'NONE', *, *, #95584, .F. ) ;
#93734=DIRECTION ( 'NONE',  ( 0.000000000000000000, -0.9999999999976377785, -2.173523156925979128E-06 ) ) ;
#93735=CARTESIAN_POINT ( 'NONE',  ( -29.52287095715006160, -24.56560739788454129, 1.056161319240904728 ) ) ;
#93738=CARTESIAN_POINT ( 'NONE',  ( 15.70846742882596025, 13.54617332914617478, 11.49999999999998934 ) ) ;
#93742=ADVANCED_FACE ( 'NONE', ( #59426 ), #50819, .T. ) ;
#93743=CARTESIAN_POINT ( 'NONE',  ( -41.55302297196116967, -23.96169478059712787, 10.65365249895718591 ) ) ;
#93744=B_SPLINE_CURVE_WITH_KNOTS ( 'NONE', 3,
 ( #30988, #46218, #14254, #29986 ),
 .UNSPECIFIED., .F., .F.,
 ( 4, 4 ),
 ( 0.000000000000000000, 1.000000000000000000 ),
 .UNSPECIFIED. ) ;
#93745=CARTESIAN_POINT ( 'NONE',  ( -48.52287095715004028, -23.73907113217710574, -1.053371485780553174 ) ) ;
#93749=CARTESIAN_POINT ( 'NONE',  ( -109.6228709571500559, -23.47596703998600631, 11.44779298504227860 ) ) ;
#93751=CARTESIAN_POINT ( 'NONE',  ( -92.62287095715005592, -29.50247984919015209, -1.443849546365051806 ) ) ;
#93753=CARTESIAN_POINT ( 'NONE',  ( 22.04941498731238525, 0.3350016526185666255, 11.49999999999999645 ) ) ;
#93755=CARTESIAN_POINT ( 'NONE',  ( -89.60222329899340821, -23.48786465467241058, 11.44779295918254114 ) ) ;
#93756=CARTESIAN_POINT ( 'NONE',  ( -20.69567741759225399, -9.018594580484563750, -1.500000000000002220 ) ) ;
#93758=CARTESIAN_POINT ( 'NONE',  ( 20.48634023128459347, 4.603634630958829632, 11.49999999999998934 ) ) ;
#93759=EDGE_CURVE ( 'NONE', #65481, #37559, #16085, .T. ) ;
#93761=CARTESIAN_POINT ( 'NONE',  ( -100.3686125512453344, -25.31369796955044649, 5.218484686103943559 ) ) ;
#93764=ORIENTED_EDGE ( 'NONE', *, *, #68022, .F. ) ;
#93765=EDGE_CURVE ( 'NONE', #85538, #93093, #65536, .T. ) ;
#93766=CARTESIAN_POINT ( 'NONE',  ( -80.62287095715008434, -24.62226745350438151, 0.9660975649728147374 ) ) ;
#93769=CARTESIAN_POINT ( 'NONE',  ( 6.139388171429570384, 20.22809724653347985, 11.49999999999998934 ) ) ;
#93770=PLANE ( 'NONE',  #70880 ) ;
#93771=CARTESIAN_POINT ( 'NONE',  ( -58.85623904670280382, -25.31249728293746060, 5.276660823416808199 ) ) ;
#93772=CARTESIAN_POINT ( 'NONE',  ( -121.5186340557655029, -24.51314013834315375, 0.6176544820404190617 ) ) ;
#93773=CARTESIAN_POINT ( 'NONE',  ( -51.62287095715005592, -23.47593901973091235, -1.443836447539009749 ) ) ;
#93774=CARTESIAN_POINT ( 'NONE',  ( -101.5228709571501327, -24.34917612406837861, 0.1852690917426578765 ) ) ;
#93775=CARTESIAN_POINT ( 'NONE',  ( 7.537409830304743430, 20.87355781386819942, -1.500000000000002220 ) ) ;
#93776=CARTESIAN_POINT ( 'NONE',  ( -81.55064642742604519, -24.15620529776628089, 10.23563542870661180 ) ) ;
#93777=EDGE_CURVE ( 'NONE', #61899, #99097, #17163, .T. ) ;
#93778=VERTEX_POINT ( 'NONE', #69031 ) ;
#93781=CARTESIAN_POINT ( 'NONE',  ( -40.25429027579533425, -25.30394352446274553, 5.534647984323703973 ) ) ;
#93782=CARTESIAN_POINT ( 'NONE',  ( -100.5472838704266820, -24.73486907724917927, 1.287355809206965240 ) ) ;
#93785=CARTESIAN_POINT ( 'NONE',  ( 19.40022266231057202, 1.907866353064612053, 11.49999999999998934 ) ) ;
#93786=CARTESIAN_POINT ( 'NONE',  ( 21.30238844577196389, 2.035401582669650544, -1.500000000000002220 ) ) ;
#93787=CARTESIAN_POINT ( 'NONE',  ( -62.53912049199733758, -24.51314013834316441, 0.6176544820404141767 ) ) ;
#93788=CARTESIAN_POINT ( 'NONE',  ( -60.56964542493874859, -23.48786465467241413, 11.44779295918254824 ) ) ;
#93790=CARTESIAN_POINT ( 'NONE',  ( -100.9649361822203133, -25.27360005675012999, 3.436944093663774957 ) ) ;
#93791=CARTESIAN_POINT ( 'NONE',  ( 16.14549698687068968, 15.95341496147077720, -1.500000000000002220 ) ) ;
#93793=B_SPLINE_CURVE_WITH_KNOTS ( 'NONE', 3,
 ( #64459, #55828, #2536, #25860, #78623, #56834, #17243, #63957, #24358, #71044, #47707, #87767, #48211, #18249 ),
 .UNSPECIFIED., .F., .F.,
 ( 4, 2, 2, 2, 2, 2, 4 ),
 ( 1.734723475976807094E-18, 0.0001838431575664456984, 0.0003676863151328896621, 0.0007353726302657787820, 0.001103058945398667848, 0.001286902102965092973, 0.001470745260531517882 ),
 .UNSPECIFIED. ) ;
#93795=CARTESIAN_POINT ( 'NONE',  ( -98.62287095715005592, -24.34917612406837861, 0.1852690917426657036 ) ) ;
#93796=CARTESIAN_POINT ( 'NONE',  ( -10.37884456512175291, 16.95428827495986823, 11.49999999999999645 ) ) ;
#93797=FACE_OUTER_BOUND ( 'NONE', #22514, .T. ) ;
#93799=CARTESIAN_POINT ( 'NONE',  ( -88.62287095715004170, -24.64898659630367916, 1.056161002820827921 ) ) ;
#93800=B_SPLINE_CURVE_WITH_KNOTS ( 'NONE', 3,
 ( #77931, #8443, #39392, #70346 ),
 .UNSPECIFIED., .F., .F.,
 ( 4, 4 ),
 ( 0.6902788356978080131, 0.6992852669699235468 ),
 .UNSPECIFIED. ) ;
#93801=DIRECTION ( 'NONE',  ( -3.773278334453079030E-23, 0.9999999999976377785, 2.173523156925979128E-06 ) ) ;
#93802=VERTEX_POINT ( 'NONE', #99959 ) ;
#93804=FACE_OUTER_BOUND ( 'NONE', #47268, .T. ) ;
#93805=CARTESIAN_POINT ( 'NONE',  ( -117.5228709571500332, -24.66019654487200441, 8.947790411086108620 ) ) ;
#93806=CARTESIAN_POINT ( 'NONE',  ( 2.849777056880220982, 21.50153301832798647, -1.500000000000002220 ) ) ;
#93807=CARTESIAN_POINT ( 'NONE',  ( -56.63256087942864525, -24.35071581493543391, 9.817618358456030592 ) ) ;
#93809=CARTESIAN_POINT ( 'NONE',  ( 19.32586673001642197, -2.567307930040524599, -1.500000000000002220 ) ) ;
#93810=CARTESIAN_POINT ( 'NONE',  ( -55.57509330567962991, -25.00182538069146432, 7.747789668545041586 ) ) ;
#93812=ORIENTED_EDGE ( 'NONE', *, *, #37526, .T. ) ;
#93813=AXIS2_PLACEMENT_3D ( 'NONE', #65658, #71248, #57539 ) ;
#93814=CARTESIAN_POINT ( 'NONE',  ( 7.100489274569507181, 19.11111018586187527, 11.49999999999999645 ) ) ;
#93815=CARTESIAN_POINT ( 'NONE',  ( -80.62512171223323776, -24.92564183028979130, 1.928384488918253536 ) ) ;
#93816=EDGE_CURVE ( 'NONE', #43961, #63898, #86176, .T. ) ;
#93818=VERTEX_POINT ( 'NONE', #53819 ) ;
#93819=CARTESIAN_POINT ( 'NONE',  ( -40.94445540056845800, -25.20887482615457742, 3.394058116165219907 ) ) ;
#93821=CARTESIAN_POINT ( 'NONE',  ( -48.87464133331025806, -25.25214680837418868, 6.106125007117622516 ) ) ;
#93822=VECTOR ( 'NONE', #59794, 1000.000000000000114 ) ;
#93823=CARTESIAN_POINT ( 'NONE',  ( -40.64047108292161425, -24.52399227489126687, 9.353111116836521077 ) ) ;
#93824=CARTESIAN_POINT ( 'NONE',  ( -52.62287095715005592, -24.64898659630367561, 1.056161002820821038 ) ) ;
#93825=CARTESIAN_POINT ( 'NONE',  ( 19.93115673323400117, -2.579441489355707606, -1.500000000000002220 ) ) ;
#93828=CARTESIAN_POINT ( 'NONE',  ( -109.5940810882278100, -23.73766607897670156, -1.055555164236452681 ) ) ;
#93831=CARTESIAN_POINT ( 'NONE',  ( 16.68310095749102118, 15.68496000196893370, 11.49999999999999645 ) ) ;
#93832=CARTESIAN_POINT ( 'NONE',  ( -10.65177407370799045, -20.06881281718593613, -1.500000000000002220 ) ) ;
#93833=VERTEX_POINT ( 'NONE', #13232 ) ;
#93834=CARTESIAN_POINT ( 'NONE',  ( -30.47287095715006799, -25.10154806753639889, 7.245676043324505322 ) ) ;
#93835=CARTESIAN_POINT ( 'NONE',  ( -96.52287095715006160, -29.50250786944525672, 11.44777988621623166 ) ) ;
#93836=CARTESIAN_POINT ( 'NONE',  ( -40.14865555004231368, -25.20037933810821684, 3.331970962322966301 ) ) ;
#93837=CARTESIAN_POINT ( 'NONE',  ( -30.57287095715006586, -24.92127980078614158, 8.082355342557208999 ) ) ;
#93838=CARTESIAN_POINT ( 'NONE',  ( -128.6243654585905176, -23.48786465467241769, 11.44779295918253403 ) ) ;
#93841=ORIENTED_EDGE ( 'NONE', *, *, #90424, .F. ) ;
#93842=CARTESIAN_POINT ( 'NONE',  ( 19.91419669613914678, 4.404666692190684962, -1.500000000000002220 ) ) ;
#93843=ORIENTED_EDGE ( 'NONE', *, *, #3401, .F. ) ;
#93844=B_SPLINE_CURVE_WITH_KNOTS ( 'NONE', 3,
 ( #83359, #28583, #37197, #28093, #74262, #44819, #99077, #45317, #67167, #5246, #37690, #44323, #30070, #50936 ),
 .UNSPECIFIED., .F., .F.,
 ( 4, 2, 2, 2, 2, 2, 4 ),
 ( 4.336808689942017736E-18, 0.0002426843972675349858, 0.0004853687945350656347, 0.0009707375890701099106, 0.001456106383605154132, 0.001698790780872676135, 0.001941475178140198571 ),
 .UNSPECIFIED. ) ;
#93845=CARTESIAN_POINT ( 'NONE',  ( -21.75629724252761577, 7.406401271465676395, -1.500000000000002220 ) ) ;
#93847=PLANE ( 'NONE',  #51738 ) ;
#93849=CARTESIAN_POINT ( 'NONE',  ( -126.5228709571500616, -29.50248528299804818, 1.056150453629047137 ) ) ;
#93851=CARTESIAN_POINT ( 'NONE',  ( 21.17668642892995834, 2.279540523802085605, 11.49999999999999645 ) ) ;
#93852=ORIENTED_EDGE ( 'NONE', *, *, #83668, .T. ) ;
#93853=ORIENTED_EDGE ( 'NONE', *, *, #86992, .F. ) ;
#93854=CARTESIAN_POINT ( 'NONE',  ( -4.330935931041660858, -21.79039167146679290, 11.49999999999998934 ) ) ;
#93855=CARTESIAN_POINT ( 'NONE',  ( -7.851838630353038972, -19.11370409007043847, 11.49999999999998934 ) ) ;
#93856=ORIENTED_EDGE ( 'NONE', *, *, #86430, .T. ) ;
#93857=CARTESIAN_POINT ( 'NONE',  ( -109.5136315545911856, -25.27682841784137935, 5.394825679379001926 ) ) ;
#93858=EDGE_CURVE ( 'NONE', #79844, #42155, #52215, .T. ) ;
#93859=CARTESIAN_POINT ( 'NONE',  ( -70.78925874883387337, -25.32724624944561853, 4.398071659717722959 ) ) ;
#93860=ORIENTED_EDGE ( 'NONE', *, *, #66917, .T. ) ;
#93862=LINE ( 'NONE', #95867, #85066 ) ;
#93863=VECTOR ( 'NONE', #7339, 1000.000000000000114 ) ;
#93864=ORIENTED_EDGE ( 'NONE', *, *, #8299, .T. ) ;
#93865=CARTESIAN_POINT ( 'NONE',  ( -58.62366816843541528, -24.66019654487199730, 8.947790411086117501 ) ) ;
#93866=EDGE_CURVE ( 'NONE', #1645, #34336, #28965, .T. ) ;
#93868=CARTESIAN_POINT ( 'NONE',  ( -19.30504728598367237, -7.930543132070424051, -1.500000000000002220 ) ) ;
#93869=CARTESIAN_POINT ( 'NONE',  ( 12.58402814888991372, -17.87355554032721372, 11.49999999999999645 ) ) ;
#93871=CARTESIAN_POINT ( 'NONE',  ( -102.6228709571500843, -24.51387760970724372, 9.387446482453405849 ) ) ;
#93873=CARTESIAN_POINT ( 'NONE',  ( 22.48569338394020534, -0.9006126209707296937, 11.49999999999998934 ) ) ;
#93875=EDGE_CURVE ( 'NONE', #43355, #39879, #60441, .T. ) ;
#93877=CARTESIAN_POINT ( 'NONE',  ( -50.52287095715005449, -24.15516710230293640, 10.28746687063726029 ) ) ;
#93878=CARTESIAN_POINT ( 'NONE',  ( -78.62287095715007013, -23.48783264082478439, -1.443836473390065711 ) ) ;
#93879=ORIENTED_EDGE ( 'NONE', *, *, #26083, .T. ) ;
#93883=ORIENTED_EDGE ( 'NONE', *, *, #70858, .F. ) ;
#93884=ORIENTED_EDGE ( 'NONE', *, *, #13569, .F. ) ;
#93885=CARTESIAN_POINT ( 'NONE',  ( 3.659817510876246960, 21.07357064420920878, -1.500000000000002220 ) ) ;
#93886=CARTESIAN_POINT ( 'NONE',  ( -3.695635658436464244, 22.08213133993951161, 11.49999999999999645 ) ) ;
#93888=CARTESIAN_POINT ( 'NONE',  ( 9.758084087097168791, -18.66043984184860349, 11.49999999999998934 ) ) ;
#93889=CARTESIAN_POINT ( 'NONE',  ( -30.40154451732978913, -25.30207583497731250, 6.147639284700202822 ) ) ;
#93890=CARTESIAN_POINT ( 'NONE',  ( -8.813339738934139689, -17.91118242276673911, -1.500000000000002220 ) ) ;
#93892=CARTESIAN_POINT ( 'NONE',  ( -49.21454750704995007, -25.13877828889947352, 7.069183601642414772 ) ) ;
#93893=CARTESIAN_POINT ( 'NONE',  ( 19.14557405504459453, -10.84957060938160289, -1.500000000000002220 ) ) ;
#93894=CARTESIAN_POINT ( 'NONE',  ( -83.52287095715006160, -24.64898659630367916, 1.056161002820826145 ) ) ;
#93896=CARTESIAN_POINT ( 'NONE',  ( -30.64643901537730741, -23.50397814795999096, 11.46586199002818418 ) ) ;
#93897=CARTESIAN_POINT ( 'NONE',  ( -54.58953762381671737, -23.47596703998600276, 11.44779298504227505 ) ) ;
#93898=CARTESIAN_POINT ( 'NONE',  ( -20.61801493038525379, 2.926015819835423581, 11.49999999999999645 ) ) ;
#93902=CARTESIAN_POINT ( 'NONE',  ( -6.620899627221215944, -20.26055204357936290, 11.49999999999998934 ) ) ;
#93903=DIRECTION ( 'NONE',  ( 1.000000000000000000, 3.773278334444167608E-23, 8.201307833595939069E-29 ) ) ;
#93905=DIRECTION ( 'NONE',  ( 0.000000000000000000, -2.173523156925979552E-06, 0.9999999999976378895 ) ) ;
#93907=CARTESIAN_POINT ( 'NONE',  ( -17.96456891314058879, -13.58578184957126034, -1.500000000000002220 ) ) ;
#93910=CARTESIAN_POINT ( 'NONE',  ( -79.39735417168856202, -25.30496935757056676, 4.861733025172510381 ) ) ;
#93912=CARTESIAN_POINT ( 'NONE',  ( 13.13437215454093199, 14.66711140016434278, 11.49999999999999645 ) ) ;
#93913=CARTESIAN_POINT ( 'NONE',  ( -55.62287095715004170, -25.00182538069145011, 7.747789668545097541 ) ) ;
#93914=DIRECTION ( 'NONE',  ( -1.000000000000000000, -3.773278334444167608E-23, -8.201307837791369499E-29 ) ) ;
#93915=ORIENTED_EDGE ( 'NONE', *, *, #42293, .F. ) ;
#93916=CARTESIAN_POINT ( 'NONE',  ( -99.51916590676324859, -23.73766607897671577, -1.055555164236429366 ) ) ;
#93917=CARTESIAN_POINT ( 'NONE',  ( -55.62287095715005592, -23.84047902841601285, -0.8780736468305797571 ) ) ;
#93918=CARTESIAN_POINT ( 'NONE',  ( -30.57287095715006231, -23.47594215783195537, -5.102550391006585557E-05 ) ) ;
#93919=EDGE_CURVE ( 'NONE', #61427, #71750, #89776, .T. ) ;
#93921=CARTESIAN_POINT ( 'NONE',  ( -0.9724026449420489771, -19.73431249065222204, -1.500000000000002220 ) ) ;
#93922=ORIENTED_EDGE ( 'NONE', *, *, #13692, .T. ) ;
#93923=CARTESIAN_POINT ( 'NONE',  ( 15.73562052650688514, -12.66937975264744587, 11.49999999999999645 ) ) ;
#93926=EDGE_CURVE ( 'NONE', #89711, #20834, #40596, .T. ) ;
#93928=ADVANCED_FACE ( 'NONE', ( #39078 ), #23438, .T. ) ;
#93930=CARTESIAN_POINT ( 'NONE',  ( -107.6228709571500843, -24.51283580621364422, 0.6167428607019860287 ) ) ;
#93931=CARTESIAN_POINT ( 'NONE',  ( -65.52287095715006160, -23.48786465467241058, 11.44779295918254647 ) ) ;
#93932=CARTESIAN_POINT ( 'NONE',  ( -59.62287095715006302, -23.48786465467241058, 11.44779295918254824 ) ) ;
#93934=VECTOR ( 'NONE', #21932, 1000.000000000000114 ) ;
#93935=CARTESIAN_POINT ( 'NONE',  ( -79.62287095715005592, -29.50248528299804818, 1.056150453629038477 ) ) ;
#93936=DIRECTION ( 'NONE',  ( 1.000000000000000000, 3.773278334444167608E-23, 8.201307833595939069E-29 ) ) ;
#93937=CARTESIAN_POINT ( 'NONE',  ( -18.86779840422491716, -6.689013621249945807, 11.49999999999998934 ) ) ;
#93938=CARTESIAN_POINT ( 'NONE',  ( -99.77116551335946326, -25.27532895947881642, 2.990445617998676031 ) ) ;
#93939=CARTESIAN_POINT ( 'NONE',  ( -45.52197096335316928, -23.48786465467240347, 11.44779295918255002 ) ) ;
#93944=CARTESIAN_POINT ( 'NONE',  ( -109.3750630267952317, -25.18430312985891462, 4.026263409152782025 ) ) ;
#93945=DIRECTION ( 'NONE',  ( -3.773278334453079030E-23, 0.9999999999976377785, 2.173523156925979128E-06 ) ) ;
#93946=FACE_OUTER_BOUND ( 'NONE', #16894, .T. ) ;
#93949=CARTESIAN_POINT ( 'NONE',  ( -83.59947554517194135, -23.73766607897670511, -1.055555164236457122 ) ) ;
#93952=CARTESIAN_POINT ( 'NONE',  ( -73.62287095715007013, -23.73907113216990794, -1.053371485793229700 ) ) ;
#93953=ORIENTED_EDGE ( 'NONE', *, *, #86761, .T. ) ;
#93954=CARTESIAN_POINT ( 'NONE',  ( 6.844040470191356640, -19.11863935190610064, 11.49999999999998934 ) ) ;
#93956=CARTESIAN_POINT ( 'NONE',  ( -59.65601704802426752, -23.48786465467240703, 11.44779295918255180 ) ) ;
#93959=CARTESIAN_POINT ( 'NONE',  ( -94.55620429048339304, -23.47596703998600631, 11.44779298504227683 ) ) ;
#93960=CARTESIAN_POINT ( 'NONE',  ( 19.60372117168125072, 4.849774137724135237, -1.500000000000002220 ) ) ;
#93961=CARTESIAN_POINT ( 'NONE',  ( 20.71511372717374755, 4.256074106246791722, 11.49999999999999645 ) ) ;
#93962=CARTESIAN_POINT ( 'NONE',  ( -19.88706384024380824, 9.709922325909349894, -1.500000000000002220 ) ) ;
#93963=CARTESIAN_POINT ( 'NONE',  ( -14.18348626307465743, -14.89297910716571849, -1.500000000000002220 ) ) ;
#93964=B_SPLINE_CURVE_WITH_KNOTS ( 'NONE', 3,
 ( #36685, #51919, #83347, #67650, #27082, #52414 ),
 .UNSPECIFIED., .F., .F.,
 ( 4, 2, 4 ),
 ( 0.000000000000000000, 0.001380901958385387894, 0.002761803916770775788 ),
 .UNSPECIFIED. ) ;
#93965=DIRECTION ( 'NONE',  ( -3.773278334453079030E-23, 0.9999999999976377785, 2.173523156925979128E-06 ) ) ;
#93967=CARTESIAN_POINT ( 'NONE',  ( -116.5562042904833646, -24.64965694238575011, 8.947790433994187609 ) ) ;
#93968=ORIENTED_EDGE ( 'NONE', *, *, #98126, .T. ) ;
#93969=FACE_OUTER_BOUND ( 'NONE', #20248, .T. ) ;
#93970=CARTESIAN_POINT ( 'NONE',  ( -110.6228709571501128, -24.63345952396255356, 9.038047939301508293 ) ) ;
#93974=VERTEX_POINT ( 'NONE', #39583 ) ;
#93975=CARTESIAN_POINT ( 'NONE',  ( -103.6228709571500559, -23.48786465467241769, 11.44779295918254114 ) ) ;
#93976=FACE_OUTER_BOUND ( 'NONE', #97637, .T. ) ;
#93978=CARTESIAN_POINT ( 'NONE',  ( 12.98984941077313415, -16.12360325096057423, -1.500000000000002220 ) ) ;
#93979=CARTESIAN_POINT ( 'NONE',  ( 13.45394552336293614, 17.01807010946250287, 11.49999999999999645 ) ) ;
#93982=LINE ( 'NONE', #84372, #41829 ) ;
#93984=CARTESIAN_POINT ( 'NONE',  ( -17.59303920844588376, -13.82112144285918731, -1.500000000000002220 ) ) ;
#93985=EDGE_CURVE ( 'NONE', #80499, #41151, #54745, .T. ) ;
#93986=CARTESIAN_POINT ( 'NONE',  ( -47.55322324058889194, -23.96169478059712432, 10.65365249895718591 ) ) ;
#93987=FACE_OUTER_BOUND ( 'NONE', #20362, .T. ) ;
#93988=EDGE_LOOP ( 'NONE', ( #38963, #25045, #24589, #51933 ) ) ;
#93989=CARTESIAN_POINT ( 'NONE',  ( -35.57452074104147499, -23.48786465467240347, 11.44779295918255180 ) ) ;
#93990=EDGE_CURVE ( 'NONE', #10184, #89509, #91024, .T. ) ;
#93992=ORIENTED_EDGE ( 'NONE', *, *, #9386, .T. ) ;
#93993=VECTOR ( 'NONE', #76860, 1000.000000000000114 ) ;
#93994=CARTESIAN_POINT ( 'NONE',  ( -70.52287095715007581, -23.48783264082477018, -1.443836473390089914 ) ) ;
#93996=B_SPLINE_CURVE_WITH_KNOTS ( 'NONE', 3,
 ( #42611, #96880, #27372, #58332, #19737, #84520, #30230, #53094 ),
 .UNSPECIFIED., .F., .F.,
 ( 4, 2, 2, 4 ),
 ( -0.001240666984356060716, -0.0002401179793396601269, 0.0007604310256767404623, 0.002761529035709539039 ),
 .UNSPECIFIED. ) ;
#93997=CARTESIAN_POINT ( 'NONE',  ( -101.2228709571500644, -23.47596703998600631, 11.44779298504227683 ) ) ;
#93998=CARTESIAN_POINT ( 'NONE',  ( -6.524719417830534773, 20.15472526627327454, -1.500000000000002220 ) ) ;
#94000=CARTESIAN_POINT ( 'NONE',  ( -50.64241578966740320, -24.40034930558991277, 0.3402023900116070698 ) ) ;
#94001=CARTESIAN_POINT ( 'NONE',  ( -6.457742198559264679, -20.83860622980983024, -1.500000000000002220 ) ) ;
#94005=CARTESIAN_POINT ( 'NONE',  ( -116.6228709571500559, -24.65952944569305316, 1.056160979905706121 ) ) ;
#94006=CARTESIAN_POINT ( 'NONE',  ( -21.69466673205137752, 2.402554924997643226, -1.500000000000002220 ) ) ;
#94007=CARTESIAN_POINT ( 'NONE',  ( -95.52287095715007581, -24.15431212366388536, -0.2830839119429101047 ) ) ;
#94012=EDGE_LOOP ( 'NONE', ( #97149, #52741, #27227, #93116 ) ) ;
#94014=CARTESIAN_POINT ( 'NONE',  ( -110.0174630698386693, -25.31122420432532394, 5.385070121809086174 ) ) ;
#94015=ORIENTED_EDGE ( 'NONE', *, *, #21227, .T. ) ;
#94018=CARTESIAN_POINT ( 'NONE',  ( -27.75920500495050192, -24.77795200822517430, 2.278718183652751250 ) ) ;
#94019=AXIS2_PLACEMENT_3D ( 'NONE', #26343, #64436, #65929 ) ;
#94020=CARTESIAN_POINT ( 'NONE',  ( -120.5228709571500616, -23.47593901973090524, -1.443836447538996204 ) ) ;
#94021=CARTESIAN_POINT ( 'NONE',  ( 14.73992482348874411, 15.29747818672187165, -1.500000000000002220 ) ) ;
#94023=FACE_OUTER_BOUND ( 'NONE', #32714, .T. ) ;
#94024=FACE_OUTER_BOUND ( 'NONE', #54658, .T. ) ;
#94025=CARTESIAN_POINT ( 'NONE',  ( -40.62287095715005592, -23.48786465467240347, 11.44779295918255180 ) ) ;
#94026=AXIS2_PLACEMENT_3D ( 'NONE', #70574, #17793, #47242 ) ;
#94027=CARTESIAN_POINT ( 'NONE',  ( 19.37663158793545293, -0.8356294931911363300, -1.500000000000002220 ) ) ;
#94028=LINE ( 'NONE', #26021, #55529 ) ;
#94029=VERTEX_POINT ( 'NONE', #18248 ) ;
#94030=CARTESIAN_POINT ( 'NONE',  ( 19.40022266231057202, 1.907866353064612053, 11.49999999999999645 ) ) ;
#94032=CARTESIAN_POINT ( 'NONE',  ( -79.49204124755721068, -25.20847803697028411, 6.537282351667380809 ) ) ;
#94033=EDGE_CURVE ( 'NONE', #40045, #25965, #82584, .T. ) ;
#94034=ORIENTED_EDGE ( 'NONE', *, *, #54540, .T. ) ;
#94036=CARTESIAN_POINT ( 'NONE',  ( -89.52215898723319754, -23.48783264082478084, -1.443836473390068598 ) ) ;
#94037=CARTESIAN_POINT ( 'NONE',  ( -91.62287095714998486, -24.33927499327853639, 9.819080762295815390 ) ) ;
#94040=CARTESIAN_POINT ( 'NONE',  ( -18.74838588596843181, -5.942601993926947657, -1.500000000000002220 ) ) ;
#94041=ORIENTED_EDGE ( 'NONE', *, *, #8029, .F. ) ;
#94042=CARTESIAN_POINT ( 'NONE',  ( 21.32721141102669193, -3.434809268862642817, -1.500000000000002220 ) ) ;
#94043=CARTESIAN_POINT ( 'NONE',  ( -85.52287095715003318, -25.00182538069145011, 7.747789668545101094 ) ) ;
#94045=CARTESIAN_POINT ( 'NONE',  ( 8.651921485055520833, -21.43433228965458781, -1.500000000000002220 ) ) ;
#94046=ADVANCED_FACE ( 'NONE', ( #80148 ), #15340, .T. ) ;
#94048=EDGE_CURVE ( 'NONE', #93616, #19525, #45641, .T. ) ;
#94052=CARTESIAN_POINT ( 'NONE',  ( -104.5228709571500474, -24.33927499327855060, 9.819080762295804732 ) ) ;
#94053=CARTESIAN_POINT ( 'NONE',  ( -110.8797149084312537, -25.29823833487873586, 2.935127919112444861 ) ) ;
#94054=CARTESIAN_POINT ( 'NONE',  ( -98.52287095715007581, -23.47593901973090524, -1.443836447538996648 ) ) ;
#94055=CARTESIAN_POINT ( 'NONE',  ( -114.5511084051358921, -24.66019654487200441, 8.947790411086106843 ) ) ;
#94056=CARTESIAN_POINT ( 'NONE',  ( 5.901097582950029619, 19.04237314665466485, -1.500000000000002220 ) ) ;
#94057=CARTESIAN_POINT ( 'NONE',  ( -75.55240587615696768, -24.15602025860895807, 10.28564288303536678 ) ) ;
#94058=CARTESIAN_POINT ( 'NONE',  ( -12.90690225449951001, 15.05119527412115055, -1.500000000000002220 ) ) ;
#94059=ORIENTED_EDGE ( 'NONE', *, *, #28413, .T. ) ;
#94060=CARTESIAN_POINT ( 'NONE',  ( -56.50842078106121136, -23.96119346886880663, -0.6495511937832126881 ) ) ;
#94061=CARTESIAN_POINT ( 'NONE',  ( -123.5562042904833930, -23.47596703998600631, 11.44779298504227683 ) ) ;
#94063=CARTESIAN_POINT ( 'NONE',  ( -6.500255983836059848, -19.66680810221124887, 11.49999999999999645 ) ) ;
#94064=DIRECTION ( 'NONE',  ( -3.773278334453080206E-23, 0.9999999999976377785, 2.173523156925979975E-06 ) ) ;
#94067=CARTESIAN_POINT ( 'NONE',  ( -40.58953762381673158, -24.99132157543083466, 2.256160258750496084 ) ) ;
#94068=CARTESIAN_POINT ( 'NONE',  ( 21.73672277138745201, -6.736064506363727666, 11.49999999999999645 ) ) ;
#94070=CARTESIAN_POINT ( 'NONE',  ( -69.65141362638318867, -23.48783264082476308, -1.443836473390097908 ) ) ;
#94071=CARTESIAN_POINT ( 'NONE',  ( -100.5228709571500616, -29.50248789122583659, 2.256150453626215580 ) ) ;
#94073=B_SPLINE_CURVE_WITH_KNOTS ( 'NONE', 3,
 ( #87126, #17618, #48590, #79513, #64325, #95242 ),
 .UNSPECIFIED., .F., .F.,
 ( 4, 2, 4 ),
 ( 1.570887131794638196E-05, 0.001396322306279761073, 0.002776935741241575838 ),
 .UNSPECIFIED. ) ;
#94074=CARTESIAN_POINT ( 'NONE',  ( 4.066846734877469949, -19.79409818376439389, 11.49999999999998934 ) ) ;
#94075=CARTESIAN_POINT ( 'NONE',  ( -50.62287095715005592, -29.50250786944525672, 11.44777988621624054 ) ) ;
#94076=CARTESIAN_POINT ( 'NONE',  ( -53.52287095715006870, -29.50248528299804818, 1.056150453629033370 ) ) ;
#94077=ORIENTED_EDGE ( 'NONE', *, *, #44090, .F. ) ;
#94078=CARTESIAN_POINT ( 'NONE',  ( -0.1447610318486398373, -21.17595468364151046, -1.479945482512687427 ) ) ;
#94079=CARTESIAN_POINT ( 'NONE',  ( -17.45619364963476627, 14.87644265977633573, 11.49999999999998934 ) ) ;
#94080=CARTESIAN_POINT ( 'NONE',  ( -40.53036611195729222, -25.12111198278256552, 2.835794650103506509 ) ) ;
#94082=CARTESIAN_POINT ( 'NONE',  ( -18.86779840422491716, -6.689013621249945807, -1.500000000000002220 ) ) ;
#94083=CARTESIAN_POINT ( 'NONE',  ( -104.6228709571500985, -23.96127896941632685, -0.6493128931037839280 ) ) ;
#94084=CARTESIAN_POINT ( 'NONE',  ( -12.59924929152775874, 16.77720732749412846, 11.49999999999999645 ) ) ;
#94085=VECTOR ( 'NONE', #7489, 1000.000000000000114 ) ;
#94087=CARTESIAN_POINT ( 'NONE',  ( -124.5545015191503637, -24.51314013834317151, 0.6176544820404232805 ) ) ;
#94088=CARTESIAN_POINT ( 'NONE',  ( -20.57682416348112397, 7.868404785394932155, 11.49999999999998934 ) ) ;
#94090=ORIENTED_EDGE ( 'NONE', *, *, #38663, .F. ) ;
#94091=PLANE ( 'NONE',  #71758 ) ;
#94094=PLANE ( 'NONE',  #64799 ) ;
#94095=ORIENTED_EDGE ( 'NONE', *, *, #49391, .T. ) ;
#94098=CARTESIAN_POINT ( 'NONE',  ( -118.5895376238167387, -24.66019654487200086, 8.947790411086119278 ) ) ;
#94100=CARTESIAN_POINT ( 'NONE',  ( -36.62372823607387318, -24.65952944569304606, 1.056160979905696129 ) ) ;
#94101=CARTESIAN_POINT ( 'NONE',  ( 16.50020720150075348, -12.08490501797973238, -1.500000000000002220 ) ) ;
#94102=ORIENTED_EDGE ( 'NONE', *, *, #54881, .F. ) ;
#94104=CARTESIAN_POINT ( 'NONE',  ( -44.61592860413497874, -23.48783264082476663, -1.443836473390094799 ) ) ;
#94106=CARTESIAN_POINT ( 'NONE',  ( -19.83904684311861644, 10.14288308415042827, 11.49999999999998934 ) ) ;
#94107=CARTESIAN_POINT ( 'NONE',  ( -38.62287095715005592, -29.50247984919015209, -1.443849546365060466 ) ) ;
#94110=B_SPLINE_CURVE_WITH_KNOTS ( 'NONE', 3,
 ( #71003, #85718, #24807, #55283 ),
 .UNSPECIFIED., .F., .F.,
 ( 4, 4 ),
 ( 0.000000000000000000, 1.000000000000000000 ),
 .UNSPECIFIED. ) ;
#94112=CARTESIAN_POINT ( 'NONE',  ( -118.5228709571500616, -23.72747288104470442, -1.053458166803224572 ) ) ;
#94114=CARTESIAN_POINT ( 'NONE',  ( -16.21995886604411297, 13.06735728859114509, 11.49999999999998934 ) ) ;
#94115=EDGE_CURVE ( 'NONE', #37822, #53379, #27915, .T. ) ;
#94117=CARTESIAN_POINT ( 'NONE',  ( -52.52287095715009713, -23.48783264083416356, -1.443836473375487151 ) ) ;
#94118=ORIENTED_EDGE ( 'NONE', *, *, #43509, .F. ) ;
#94120=CARTESIAN_POINT ( 'NONE',  ( -51.31235188911633571, -25.25854493898471276, 6.754155260380676040 ) ) ;
#94121=CARTESIAN_POINT ( 'NONE',  ( -17.33045254171255678, -11.89390297951003816, -1.500000000000002220 ) ) ;
#94123=LINE ( 'NONE', #18007, #835 ) ;
#94126=CARTESIAN_POINT ( 'NONE',  ( -86.64363164346322321, -23.48786465467240703, 11.44779295918254647 ) ) ;
#94127=CARTESIAN_POINT ( 'NONE',  ( -110.1351499245318877, -25.12167980767599929, 2.838884635434631765 ) ) ;
#94129=CARTESIAN_POINT ( 'NONE',  ( -7.477829544921322125, 20.88912457518834742, 11.49999999999999645 ) ) ;
#94130=ORIENTED_EDGE ( 'NONE', *, *, #5221, .F. ) ;
#94132=DIRECTION ( 'NONE',  ( -3.773278334453079618E-23, 0.9999999999976377785, 2.173523156925979975E-06 ) ) ;
#94133=CARTESIAN_POINT ( 'NONE',  ( -37.55620429048340014, -23.48786465467240347, 11.44779295918255180 ) ) ;
#94135=CARTESIAN_POINT ( 'NONE',  ( -16.57510365746454184, 15.48777146884464884, 11.49999999999998934 ) ) ;
#94140=VECTOR ( 'NONE', #83929, 1000.000000000000114 ) ;
#94141=CARTESIAN_POINT ( 'NONE',  ( 11.25103634530202790, -16.72154935384561725, -1.500000000000002220 ) ) ;
#94143=ORIENTED_EDGE ( 'NONE', *, *, #32273, .T. ) ;
#94145=CARTESIAN_POINT ( 'NONE',  ( -21.98280116189361877, -4.439423430357301470, -1.500000000000002220 ) ) ;
#94146=EDGE_CURVE ( 'NONE', #39688, #53441, #43766, .T. ) ;
#94149=CARTESIAN_POINT ( 'NONE',  ( -112.5880276694465181, -24.51419770103158413, 9.386484678747166299 ) ) ;
#94150=CARTESIAN_POINT ( 'NONE',  ( -94.59406235252116346, -23.96169478059713143, 10.65365249895717881 ) ) ;
#94151=DIRECTION ( 'NONE',  ( -3.773278334453080206E-23, 0.9999999999976377785, 2.173523156925979975E-06 ) ) ;
#94154=EDGE_CURVE ( 'NONE', #19978, #93020, #49896, .T. ) ;
#94155=VECTOR ( 'NONE', #57628, 1000.000000000000114 ) ;
#94156=CARTESIAN_POINT ( 'NONE',  ( 6.425176733589397671, 18.50107501292125178, 11.49999999999998934 ) ) ;
#94158=ORIENTED_EDGE ( 'NONE', *, *, #68571, .F. ) ;
#94159=CARTESIAN_POINT ( 'NONE',  ( 3.930203739357332360, 21.12693704021120666, 11.49999999999998934 ) ) ;
#94163=CARTESIAN_POINT ( 'NONE',  ( -68.62287095715005592, -24.64965695001468404, 8.947790433994184056 ) ) ;
#94164=CARTESIAN_POINT ( 'NONE',  ( 22.85142058292489153, -2.183311388647848350, -1.500000000000002220 ) ) ;
#94165=EDGE_CURVE ( 'NONE', #73557, #29958, #18425, .T. ) ;
#94166=ADVANCED_FACE ( 'NONE', ( #59879 ), #30907, .F. ) ;
#94168=CARTESIAN_POINT ( 'NONE',  ( -96.63574071546304367, -23.73791477778911840, 11.05961554403170410 ) ) ;
#94169=FACE_OUTER_BOUND ( 'NONE', #77879, .T. ) ;
#94170=CARTESIAN_POINT ( 'NONE',  ( -4.446071851354966853, 19.53225066162704948, 11.49999999999999645 ) ) ;
#94175=CARTESIAN_POINT ( 'NONE',  ( -46.62287095715004881, -24.64898659630528499, 1.056161002820821038 ) ) ;
#94176=CARTESIAN_POINT ( 'NONE',  ( 1.937016913031804455, -21.67664703184077268, -1.500000000000002220 ) ) ;
#94178=CARTESIAN_POINT ( 'NONE',  ( 6.560884470684795744, 18.50665934316380756, -1.500000000000002220 ) ) ;
#94179=DIRECTION ( 'NONE',  ( 0.000000000000000000, 2.173523156925980399E-06, -0.9999999999976378895 ) ) ;
#94180=CARTESIAN_POINT ( 'NONE',  ( -109.8661607933284472, -25.31698164407086793, 5.216081326368730231 ) ) ;
#94184=CARTESIAN_POINT ( 'NONE',  ( -14.32454646668868747, 14.77526322620295929, 11.49999999999999645 ) ) ;
#94186=CARTESIAN_POINT ( 'NONE',  ( -120.5534794319312653, -24.63355581998386157, 0.9682620441943888823 ) ) ;
#94187=EDGE_CURVE ( 'NONE', #73037, #88312, #30406, .T. ) ;
#94188=CARTESIAN_POINT ( 'NONE',  ( -22.51868310087907687, -2.221351303042197411, 11.49999999999999645 ) ) ;
#94190=CARTESIAN_POINT ( 'NONE',  ( -70.29041810236439858, -25.25639601273440249, 7.100646424425399061 ) ) ;
#94191=CARTESIAN_POINT ( 'NONE',  ( -26.38925086361725647, -24.87739167191250544, 6.668544504290081498 ) ) ;
#94192=FACE_OUTER_BOUND ( 'NONE', #49832, .T. ) ;
#94194=EDGE_CURVE ( 'NONE', #13356, #26478, #36563, .T. ) ;
#94195=CARTESIAN_POINT ( 'NONE',  ( -25.56960729154874556, -24.61459572358360859, 5.760628103071427475 ) ) ;
#94196=CARTESIAN_POINT ( 'NONE',  ( -28.52287095715007581, -23.79900956871740547, 10.65359469479120058 ) ) ;
#94199=ORIENTED_EDGE ( 'NONE', *, *, #80476, .T. ) ;
#94200=CARTESIAN_POINT ( 'NONE',  ( -80.09072421954219578, -25.31596230203514608, 5.004106418144936619 ) ) ;
#94201=CARTESIAN_POINT ( 'NONE',  ( 22.28265747778879202, 5.072132558558076099, -1.500000000000002220 ) ) ;
#94202=FACE_OUTER_BOUND ( 'NONE', #57537, .T. ) ;
#94204=CARTESIAN_POINT ( 'NONE',  ( -63.54360795143862362, -24.35071581493543036, 9.817618358456027039 ) ) ;
#94205=CARTESIAN_POINT ( 'NONE',  ( -1.726696889551340153, 22.42386595106472669, 11.49999999999999645 ) ) ;
#94206=ORIENTED_EDGE ( 'NONE', *, *, #71885, .F. ) ;
#94207=CARTESIAN_POINT ( 'NONE',  ( -34.62287095715005592, -24.33927499327853639, 9.819080762295829601 ) ) ;
#94208=B_SPLINE_CURVE_WITH_KNOTS ( 'NONE', 3,
 ( #56300, #87221, #10099, #1999 ),
 .UNSPECIFIED., .F., .F.,
 ( 4, 4 ),
 ( 0.000000000000000000, 9.999999999996123101E-05 ),
 .UNSPECIFIED. ) ;
#94209=AXIS2_PLACEMENT_3D ( 'NONE', #38267, #68732, #99163 ) ;
#94210=CARTESIAN_POINT ( 'NONE',  ( -13.81295463269534096, 17.03802364079049525, -1.500000000000002220 ) ) ;
#94212=B_SPLINE_CURVE_WITH_KNOTS ( 'NONE', 3,
 ( #40074, #6728, #72033, #79123 ),
 .UNSPECIFIED., .F., .F.,
 ( 4, 4 ),
 ( 1.387778780781445676E-17, 0.0001000000000000167422 ),
 .UNSPECIFIED. ) ;
#94213=CARTESIAN_POINT ( 'NONE',  ( -44.49964348827519700, -24.15620529776628089, 10.23563542870660470 ) ) ;
#94214=CARTESIAN_POINT ( 'NONE',  ( -99.52287095715006160, -29.50248528299804818, 1.056150453629042030 ) ) ;
#94216=CARTESIAN_POINT ( 'NONE',  ( -112.5895376238167387, -23.48786465467241769, 11.44779295918254114 ) ) ;
#94218=VERTEX_POINT ( 'NONE', #78565 ) ;
#94219=CARTESIAN_POINT ( 'NONE',  ( 1.259202695315177589, 20.44674571593545664, -1.500000000000002220 ) ) ;
#94220=ORIENTED_EDGE ( 'NONE', *, *, #31399, .F. ) ;
#94221=VERTEX_POINT ( 'NONE', #70479 ) ;
#94223=VERTEX_POINT ( 'NONE', #38020 ) ;
#94225=CARTESIAN_POINT ( 'NONE',  ( 22.94779996701378266, 2.684060219229261968, -1.500000000000002220 ) ) ;
#94226=CARTESIAN_POINT ( 'NONE',  ( -112.5228709571500758, -24.51387760970726148, 9.387446482453407626 ) ) ;
#94227=CARTESIAN_POINT ( 'NONE',  ( -19.77321833943668850, 4.698914572609424134, -1.500000000000002220 ) ) ;
#94229=CARTESIAN_POINT ( 'NONE',  ( -85.62287095715004170, -29.50249982740957577, 7.747779886224967605 ) ) ;
#94231=B_SPLINE_CURVE_WITH_KNOTS ( 'NONE', 3,
 ( #99899, #45644, #98915, #82696, #99414, #29909 ),
 .UNSPECIFIED., .F., .F.,
 ( 4, 2, 4 ),
 ( 0.000000000000000000, 0.001380901958385394833, 0.002761803916770789666 ),
 .UNSPECIFIED. ) ;
#94233=CARTESIAN_POINT ( 'NONE',  ( -44.55620429048339304, -24.66019654487199020, 8.947790411086137041 ) ) ;
#94235=CARTESIAN_POINT ( 'NONE',  ( 11.78165356204951131, -17.99452314462042324, 11.49999999999999645 ) ) ;
#94237=CARTESIAN_POINT ( 'NONE',  ( -75.51431064661339576, -23.85016227208580730, -0.8807180028928284221 ) ) ;
#94238=CARTESIAN_POINT ( 'NONE',  ( -104.6228709571500559, -24.64898659630529210, 1.056161002820829697 ) ) ;
#94240=ORIENTED_EDGE ( 'NONE', *, *, #10773, .F. ) ;
#94241=CARTESIAN_POINT ( 'NONE',  ( 16.28047541435887879, -12.87082401369967677, -1.500000000000002220 ) ) ;
#94243=ORIENTED_EDGE ( 'NONE', *, *, #79079, .T. ) ;
#94244=CARTESIAN_POINT ( 'NONE',  ( -125.6264014075705546, -23.48783264082478794, -1.443836473390061936 ) ) ;
#94246=EDGE_CURVE ( 'NONE', #62582, #45335, #72893, .T. ) ;
#94247=CARTESIAN_POINT ( 'NONE',  ( -111.6303196403976727, -23.73791477778912551, 11.05961554403170055 ) ) ;
#94252=CARTESIAN_POINT ( 'NONE',  ( -42.64093939733596272, -24.15620529776628089, 10.23563542870661358 ) ) ;
#94253=CARTESIAN_POINT ( 'NONE',  ( -43.53437882689529204, -24.51419770103157347, 9.386484678747182286 ) ) ;
#94254=CARTESIAN_POINT ( 'NONE',  ( 4.628415685485613551, -21.52068878818806752, 11.49999999999999645 ) ) ;
#94257=CARTESIAN_POINT ( 'NONE',  ( -8.190886813464794969, 21.05079722441571732, -1.500000000000002220 ) ) ;
#94258=CARTESIAN_POINT ( 'NONE',  ( 20.92198360912786015, -1.804805560479522342, 11.49999999999998934 ) ) ;
#94259=EDGE_CURVE ( 'NONE', #29559, #80701, #8724, .T. ) ;
#94260=CARTESIAN_POINT ( 'NONE',  ( -62.52287095715006160, -24.33832256527049154, 0.1851278514138569864 ) ) ;
#94262=ORIENTED_EDGE ( 'NONE', *, *, #92157, .T. ) ;
#94263=CARTESIAN_POINT ( 'NONE',  ( -69.55126625704997423, -29.50248967467915051, 3.076686136236004732 ) ) ;
#94267=CARTESIAN_POINT ( 'NONE',  ( 21.14167878903947084, -0.5806874866175276706, 11.49999999999998934 ) ) ;
#94269=CARTESIAN_POINT ( 'NONE',  ( -51.92774333234893192, -25.03148468052863862, 6.302625650274440439 ) ) ;
#94273=B_SPLINE_CURVE_WITH_KNOTS ( 'NONE', 3,
 ( #44814, #83857, #75733, #7224 ),
 .UNSPECIFIED., .F., .F.,
 ( 4, 4 ),
 ( 0.000000000000000000, 9.999999999998897304E-05 ),
 .UNSPECIFIED. ) ;
#94274=CARTESIAN_POINT ( 'NONE',  ( 21.27325221474336914, 6.521069146585026566, -1.500000000000002220 ) ) ;
#94275=CARTESIAN_POINT ( 'NONE',  ( -29.81175120719462157, -25.24633111994858581, 4.942810988825437235 ) ) ;
#94276=ORIENTED_EDGE ( 'NONE', *, *, #63090, .F. ) ;
#94277=LINE ( 'NONE', #48630, #44931 ) ;
#94278=CARTESIAN_POINT ( 'NONE',  ( -86.52287095715006160, -23.48786465467241058, 11.44779295918254292 ) ) ;
#94279=CARTESIAN_POINT ( 'NONE',  ( -126.5896050762271869, -24.34968618360934300, 0.1864209137778884418 ) ) ;
#94281=CARTESIAN_POINT ( 'NONE',  ( -66.62287095715005592, -23.48786465467241058, 11.44779295918254647 ) ) ;
#94282=ADVANCED_FACE ( 'NONE', ( #62889 ), #85029, .T. ) ;
#94283=CARTESIAN_POINT ( 'NONE',  ( 19.46547125265945155, -1.073068822128883104, 11.49999999999998934 ) ) ;
#94284=CARTESIAN_POINT ( 'NONE',  ( -19.04320821261859464, -9.809917703373946196, -1.500000000000002220 ) ) ;
#94286=CARTESIAN_POINT ( 'NONE',  ( -60.59238776529559090, -24.40133493613623372, 9.663955038888268234 ) ) ;
#94287=CARTESIAN_POINT ( 'NONE',  ( -100.6228709571500559, -23.48786465467241769, 11.44779295918254114 ) ) ;
#94288=PLANE ( 'NONE',  #50649 ) ;
#94289=CARTESIAN_POINT ( 'NONE',  ( -20.37646751746074969, -10.17465561509698979, -1.500000000000002220 ) ) ;
#94292=CARTESIAN_POINT ( 'NONE',  ( 12.34629653512297409, 15.52844579862587437, 11.49999999999999645 ) ) ;
#94295=CARTESIAN_POINT ( 'NONE',  ( -64.62287095715005592, -23.47593901973091235, -1.443836447539007972 ) ) ;
#94297=CARTESIAN_POINT ( 'NONE',  ( -49.34187094658451400, -25.21537169916210885, 6.482075674763354556 ) ) ;
#94300=CARTESIAN_POINT ( 'NONE',  ( -51.52876458270549165, -25.10935885016122882, 3.420678843004004488 ) ) ;
#94301=CARTESIAN_POINT ( 'NONE',  ( 2.849777056880220982, 21.50153301832798647, 11.49999999999998934 ) ) ;
#94303=CARTESIAN_POINT ( 'NONE',  ( 6.966380261627926451, -18.21767524041069564, -1.500000000000002220 ) ) ;
#94304=CARTESIAN_POINT ( 'NONE',  ( -55.63443494932560895, -24.63419186844611275, 9.035850630976927533 ) ) ;
#94305=AXIS2_PLACEMENT_3D ( 'NONE', #67343, #83037, #3572 ) ;
#94306=B_SPLINE_CURVE_WITH_KNOTS ( 'NONE', 3,
 ( #92433, #68611, #90941, #46269 ),
 .UNSPECIFIED., .F., .F.,
 ( 4, 4 ),
 ( 0.000000000000000000, 9.999999999996123101E-05 ),
 .UNSPECIFIED. ) ;
#94307=ORIENTED_EDGE ( 'NONE', *, *, #19850, .T. ) ;
#94309=CARTESIAN_POINT ( 'NONE',  ( 15.56926775127050000, -13.18612581554039132, 11.49999999999999645 ) ) ;
#94310=CARTESIAN_POINT ( 'NONE',  ( -85.52287095715009002, -23.47593901973090524, -1.443836447538996648 ) ) ;
#94312=EDGE_CURVE ( 'NONE', #8482, #80639, #3886, .T. ) ;
#94313=EDGE_LOOP ( 'NONE', ( #31463, #55961, #30067, #19093 ) ) ;
#94314=CARTESIAN_POINT ( 'NONE',  ( -30.60993385648455956, -24.45056191361606679, 9.787827635114012992 ) ) ;
#94318=CARTESIAN_POINT ( 'NONE',  ( -86.52287095715006160, -23.48783264083431277, -1.443836473375255336 ) ) ;
#94319=CARTESIAN_POINT ( 'NONE',  ( 13.72940079880349984, -14.68433028913016791, -1.500000000000002220 ) ) ;
#94321=ORIENTED_EDGE ( 'NONE', *, *, #97082, .F. ) ;
#94322=EDGE_CURVE ( 'NONE', #75118, #13466, #81325, .T. ) ;
#94323=CARTESIAN_POINT ( 'NONE',  ( -48.62287095715004881, -29.50247984919015209, -1.443849546365058689 ) ) ;
#94324=EDGE_CURVE ( 'NONE', #4924, #55530, #40172, .T. ) ;
#94325=EDGE_CURVE ( 'NONE', #9990, #1598, #75198, .T. ) ;
#94326=CARTESIAN_POINT ( 'NONE',  ( 22.74528686061176685, 3.085755641335488964, 11.49999999999999645 ) ) ;
#94327=CARTESIAN_POINT ( 'NONE',  ( 2.440706796964721370, 22.61111150098722788, -1.500000000000002220 ) ) ;
#94328=ORIENTED_EDGE ( 'NONE', *, *, #43625, .T. ) ;
#94329=CARTESIAN_POINT ( 'NONE',  ( -31.62287095715005236, -23.47596703998600276, 11.44779298504227505 ) ) ;
#94330=CARTESIAN_POINT ( 'NONE',  ( -75.62287095715005592, -23.48786465467241058, 11.44779295918254647 ) ) ;
#94331=CARTESIAN_POINT ( 'NONE',  ( -97.92287095715006728, -23.47593901973090524, -1.443836447538996870 ) ) ;
#94332=ADVANCED_FACE ( 'NONE', ( #2472 ), #48661, .F. ) ;
#94333=CARTESIAN_POINT ( 'NONE',  ( -30.57287095715008007, -25.27567627223822555, 6.132950404913888320 ) ) ;
#94337=CARTESIAN_POINT ( 'NONE',  ( -90.62287095715004170, -23.48783264082478794, -1.443836473390063713 ) ) ;
#94340=CARTESIAN_POINT ( 'NONE',  ( 15.56926775127050000, -13.18612581554039132, 11.49999999999998934 ) ) ;
#94341=ORIENTED_EDGE ( 'NONE', *, *, #90655, .F. ) ;
#94343=CARTESIAN_POINT ( 'NONE',  ( -19.06187107478486098, -12.82570580458313003, -1.500000000000002220 ) ) ;
#94346=B_SPLINE_CURVE_WITH_KNOTS ( 'NONE', 3,
 ( #94839, #41065, #72023, #8612 ),
 .UNSPECIFIED., .F., .F.,
 ( 4, 4 ),
 ( 0.08985008422344552270, 0.09885651549556107032 ),
 .UNSPECIFIED. ) ;
#94349=ADVANCED_FACE ( 'NONE', ( #56772 ), #87703, .T. ) ;
#94350=CARTESIAN_POINT ( 'NONE',  ( -117.7765765077247693, -25.21288392202306383, 6.500954737128433969 ) ) ;
#94351=CARTESIAN_POINT ( 'NONE',  ( 20.49606604269246546, -5.804284187783010474, 11.49999999999999645 ) ) ;
#94352=ORIENTED_EDGE ( 'NONE', *, *, #38589, .T. ) ;
#94353=B_SPLINE_CURVE_WITH_KNOTS ( 'NONE', 3,
 ( #25187, #24188, #9970, #56164 ),
 .UNSPECIFIED., .F., .F.,
 ( 4, 4 ),
 ( 0.9494622744413409032, 0.9504630214821060408 ),
 .UNSPECIFIED. ) ;
#94356=CARTESIAN_POINT ( 'NONE',  ( -19.97062832128981213, -9.750827054148329509, 11.49999999999998934 ) ) ;
#94358=CARTESIAN_POINT ( 'NONE',  ( 3.034461355793923509, -20.43525710956717845, 11.49999999999998934 ) ) ;
#94360=ORIENTED_EDGE ( 'NONE', *, *, #48063, .F. ) ;
#94362=CARTESIAN_POINT ( 'NONE',  ( -95.59855507052287749, -23.85049219812686161, 10.88485053497527133 ) ) ;
#94364=CARTESIAN_POINT ( 'NONE',  ( -65.58953762381671027, -25.00158670708909625, 2.256160236439167299 ) ) ;
#94365=EDGE_LOOP ( 'NONE', ( #33606, #14711, #89393, #22120 ) ) ;
#94366=CARTESIAN_POINT ( 'NONE',  ( -129.5562042904833788, -24.65952944569305316, 1.056160979905707009 ) ) ;
#94367=CARTESIAN_POINT ( 'NONE',  ( -55.52287095715006870, -23.48786465467241058, 11.44779295918254824 ) ) ;
#94368=CARTESIAN_POINT ( 'NONE',  ( 18.75483278694074940, -9.228467059531109129, -1.500000000000002220 ) ) ;
#94369=CARTESIAN_POINT ( 'NONE',  ( -17.40403014803320758, -13.24600170205644289, 11.49999999999999645 ) ) ;
#94370=EDGE_CURVE ( 'NONE', #37559, #60977, #93344, .T. ) ;
#94371=CARTESIAN_POINT ( 'NONE',  ( -52.62287095715005592, -24.50216790748100593, 0.6166512839513587085 ) ) ;
#94373=CARTESIAN_POINT ( 'NONE',  ( 19.77564376705174709, 10.73071584254150856, -1.500000000000002220 ) ) ;
#94375=CARTESIAN_POINT ( 'NONE',  ( -118.5902638581781048, -24.15620529776628800, 10.23563542870659582 ) ) ;
#94377=AXIS2_PLACEMENT_3D ( 'NONE', #81317, #11798, #18419 ) ;
#94378=CARTESIAN_POINT ( 'NONE',  ( -54.52287095715006870, -24.65952944569304606, 1.056160979905693686 ) ) ;
#94381=ORIENTED_EDGE ( 'NONE', *, *, #5787, .T. ) ;
#94382=ORIENTED_EDGE ( 'NONE', *, *, #72637, .T. ) ;
#94383=CARTESIAN_POINT ( 'NONE',  ( -99.78066557477396259, -25.26221283775623050, 6.943018465985777432 ) ) ;
#94384=ORIENTED_EDGE ( 'NONE', *, *, #67075, .T. ) ;
#94385=CARTESIAN_POINT ( 'NONE',  ( -10.59417575825165159, 18.57464501519095279, -1.500000000000002220 ) ) ;
#94387=CARTESIAN_POINT ( 'NONE',  ( 22.31825301297700648, 1.237144038376295274, 11.49999999999999645 ) ) ;
#94390=CARTESIAN_POINT ( 'NONE',  ( -8.945158345017247825, -19.07159632999312393, 11.49999999999998934 ) ) ;
#94391=CARTESIAN_POINT ( 'NONE',  ( -30.41985448271246995, -24.82657567899210704, 8.370654131274083198 ) ) ;
#94392=CARTESIAN_POINT ( 'NONE',  ( -10.29545327866581950, 17.06371652956568852, -1.500000000000002220 ) ) ;
#94393=CARTESIAN_POINT ( 'NONE',  ( -50.48627917242625784, -24.63419186844610209, 9.035850630976920428 ) ) ;
#94395=CARTESIAN_POINT ( 'NONE',  ( -3.902479932019291553, -21.71820464621639246, -1.500000000000002220 ) ) ;
#94396=DIRECTION ( 'NONE',  ( 0.06474050504609950296, -0.8381167135261472501, -0.5416355246053439210 ) ) ;
#94397=VECTOR ( 'NONE', #87030, 1000.000000000000227 ) ;
#94399=CARTESIAN_POINT ( 'NONE',  ( -116.5926287344351806, -23.73766607897671577, -1.055555164236427590 ) ) ;
#94400=CARTESIAN_POINT ( 'NONE',  ( -121.5228709571501184, -24.33832256527049154, 0.1851278514138670062 ) ) ;
#94401=CARTESIAN_POINT ( 'NONE',  ( -20.33245250387252767, 4.503473919074798104, 11.49999999999999645 ) ) ;
#94403=CARTESIAN_POINT ( 'NONE',  ( -125.5228709571500900, -24.14406661686764366, 10.28769366194080348 ) ) ;
#94404=CARTESIAN_POINT ( 'NONE',  ( -127.5895376238167245, -23.48783264082479505, -1.443836473390056829 ) ) ;
#94405=CARTESIAN_POINT ( 'NONE',  ( -8.160016139516647726, -19.69179572373923648, 11.49999999999998934 ) ) ;
#94406=CARTESIAN_POINT ( 'NONE',  ( -122.5228709571500332, -23.48783264082477018, -1.443836473390084807 ) ) ;
#94407=FACE_OUTER_BOUND ( 'NONE', #74854, .T. ) ;
#94408=CARTESIAN_POINT ( 'NONE',  ( -108.6228709571500559, -23.47593901973091235, -1.443836447538999312 ) ) ;
#94410=CARTESIAN_POINT ( 'NONE',  ( 13.09772080625096891, 18.35129493929886380, -1.500000000000002220 ) ) ;
#94412=B_SPLINE_SURFACE_WITH_KNOTS ( 'NONE', 3, 3, ( 
 ( #94851, #84854, #79124, #46296 ),
 ( #9619, #87238, #40580, #121 ),
 ( #2023, #56319, #17735, #48703 ),
 ( #43081, #12108, #13105, #20218 ),
 ( #34962, #50688, #44572, #11611 ),
 ( #35956, #90743, #44071, #65439 ),
 ( #20719, #67419, #13605, #51189 ),
 ( #36451, #50191, #34464, #97360 ),
 ( #3519, #66925, #51689, #65935 ),
 ( #82130, #81132, #4016, #42588 ) ),
 .UNSPECIFIED., .F., .F., .F.,
 ( 4, 3, 3, 4 ),
 ( 4, 4 ),
 ( 0.0004766839783821820095, 0.1491231665100173354, 0.2234464077758349099, 0.2977696490416524844 ),
 ( 0.3495362134072145244, 0.3507572252461916285 ),
 .UNSPECIFIED. ) ;
#94416=CARTESIAN_POINT ( 'NONE',  ( -68.52287095715007581, -23.47593901973090524, -1.443836447538997092 ) ) ;
#94417=CARTESIAN_POINT ( 'NONE',  ( 19.47230031930329730, 2.946587627359682493, 11.49999999999999645 ) ) ;
#94418=CARTESIAN_POINT ( 'NONE',  ( -32.07722060962682065, -25.11966440015785196, 7.363003809050452375 ) ) ;
#94421=CARTESIAN_POINT ( 'NONE',  ( -99.63766005662118630, -23.48783264082478439, -1.443836473390062825 ) ) ;
#94423=CARTESIAN_POINT ( 'NONE',  ( -105.5228709571501327, -24.83620972994591369, 8.398175272781370992 ) ) ;
#94425=CARTESIAN_POINT ( 'NONE',  ( 17.61170953066113398, -8.936083093766256980, -1.500000000000002220 ) ) ;
#94428=CARTESIAN_POINT ( 'NONE',  ( -20.17641613807547785, 1.360797614858565874, 11.49999999999999645 ) ) ;
#94430=ORIENTED_EDGE ( 'NONE', *, *, #34432, .F. ) ;
#94433=CARTESIAN_POINT ( 'NONE',  ( -50.65677132892651713, -25.30358770098895249, 5.223192127046770494 ) ) ;
#94434=CARTESIAN_POINT ( 'NONE',  ( -83.52287095715006160, -23.47593901973090524, -1.443836447538996648 ) ) ;
#94435=EDGE_CURVE ( 'NONE', #7644, #8232, #14741, .T. ) ;
#94436=CARTESIAN_POINT ( 'NONE',  ( -124.2228709571500502, -23.47593901973090524, -1.443836447538996204 ) ) ;
#94439=CARTESIAN_POINT ( 'NONE',  ( -14.99618758923778117, -13.25627519679515665, 11.49999999999998934 ) ) ;
#94440=EDGE_CURVE ( 'NONE', #33865, #96258, #75950, .T. ) ;
#94442=CARTESIAN_POINT ( 'NONE',  ( -116.5544649402113180, -24.15620529776628800, 10.23563542870659759 ) ) ;
#94443=ORIENTED_EDGE ( 'NONE', *, *, #50984, .F. ) ;
#94445=EDGE_CURVE ( 'NONE', #10131, #92742, #65646, .T. ) ;
#94446=B_SPLINE_CURVE_WITH_KNOTS ( 'NONE', 3,
 ( #38747, #38248, #62108, #24523, #69715, #54992, #30642, #31138 ),
 .UNSPECIFIED., .F., .F.,
 ( 4, 2, 2, 4 ),
 ( -0.001224873891641426512, -0.0002244903592271102304, 0.0007758931731872060512, 0.002776660238015838614 ),
 .UNSPECIFIED. ) ;
#94449=CARTESIAN_POINT ( 'NONE',  ( -104.6228709571500559, -23.48786465467241413, 11.44779295918254114 ) ) ;
#94450=CARTESIAN_POINT ( 'NONE',  ( -109.8707484289256655, -25.29012748047656700, 3.397981883223208488 ) ) ;
#94451=CARTESIAN_POINT ( 'NONE',  ( -35.46877372516544824, -24.92564183028978775, 1.928384488918258199 ) ) ;
#94452=CARTESIAN_POINT ( 'NONE',  ( -100.5228709571500900, -24.63345952396255711, 9.038047939301508293 ) ) ;
#94453=CARTESIAN_POINT ( 'NONE',  ( -117.0508430453642887, -25.34741532608440551, 3.801652799235187175 ) ) ;
#94455=CARTESIAN_POINT ( 'NONE',  ( -49.50841769935764347, -25.26288593538659910, 3.984447754961206734 ) ) ;
#94456=VECTOR ( 'NONE', #85195, 1000.000000000000114 ) ;
#94458=CARTESIAN_POINT ( 'NONE',  ( -49.76238219317473721, -25.21081864179584997, 3.487169982528662615 ) ) ;
#94460=CARTESIAN_POINT ( 'NONE',  ( 14.62039552936377085, -14.08751720214925207, 11.49999999999998934 ) ) ;
#94461=VECTOR ( 'NONE', #63326, 1000.000000000000114 ) ;
#94463=CARTESIAN_POINT ( 'NONE',  ( -34.63527674217913699, -24.34968618360933590, 0.1864209137778841396 ) ) ;
#94464=CARTESIAN_POINT ( 'NONE',  ( -105.6228709571500417, -23.85196035786902513, -0.8779234886474873711 ) ) ;
#94465=ORIENTED_EDGE ( 'NONE', *, *, #23672, .T. ) ;
#94466=CARTESIAN_POINT ( 'NONE',  ( -83.62287095715007013, -23.48786465467241769, 11.44779295918254469 ) ) ;
#94467=CARTESIAN_POINT ( 'NONE',  ( 13.66866334921533799, -14.80927461459226890, -1.500000000000002220 ) ) ;
#94469=CARTESIAN_POINT ( 'NONE',  ( -1.424071398598787397, -21.11453822904667277, 11.49999999999999645 ) ) ;
#94470=CARTESIAN_POINT ( 'NONE',  ( 14.67205787815721862, 16.58792043909384262, -1.500000000000002220 ) ) ;
#94471=CARTESIAN_POINT ( 'NONE',  ( -1.452656003914881477, -20.50939586048694352, 11.49999999999998934 ) ) ;
#94472=CARTESIAN_POINT ( 'NONE',  ( -78.92287095715005307, -23.47596703998600631, 11.44779298504227860 ) ) ;
#94473=ORIENTED_EDGE ( 'NONE', *, *, #79700, .F. ) ;
#94475=VERTEX_POINT ( 'NONE', #51134 ) ;
#94479=ORIENTED_EDGE ( 'NONE', *, *, #23665, .T. ) ;
#94481=CARTESIAN_POINT ( 'NONE',  ( -81.62287095715005592, -24.64965695001468404, 8.947790433994182280 ) ) ;
#94482=CARTESIAN_POINT ( 'NONE',  ( -91.94687923781918926, -25.23397913219354649, 6.409327625488847602 ) ) ;
#94484=CARTESIAN_POINT ( 'NONE',  ( 15.58315679939408582, 13.61395703526229894, -1.500000000000002220 ) ) ;
#94485=CARTESIAN_POINT ( 'NONE',  ( 21.56569437331729233, -1.927008741106717604, 11.49999999999999645 ) ) ;
#94487=CARTESIAN_POINT ( 'NONE',  ( -62.58953762381672448, -24.65952944569303895, 1.056160979905689024 ) ) ;
#94488=CARTESIAN_POINT ( 'NONE',  ( -28.55620429048338593, -23.32635600711839885, 11.44779298526909983 ) ) ;
#94489=CARTESIAN_POINT ( 'NONE',  ( 10.13505985054399083, -19.98934331558005439, -1.500000000000002220 ) ) ;
#94491=CARTESIAN_POINT ( 'NONE',  ( -47.50672211067188044, -23.96169478059712432, 10.65365249895718591 ) ) ;
#94495=CARTESIAN_POINT ( 'NONE',  ( -114.6228709571500417, -23.48786465467241769, 11.44779295918253936 ) ) ;
#94499=B_SPLINE_CURVE_WITH_KNOTS ( 'NONE', 3,
 ( #36590, #29469, #75640, #59442, #89386, #19859, #82269, #12745 ),
 .UNSPECIFIED., .F., .F.,
 ( 4, 2, 2, 4 ),
 ( -0.001240666984355839756, -0.0002401179793394981471, 0.0007604310256768434615, 0.002761529035709530365 ),
 .UNSPECIFIED. ) ;
#94501=CARTESIAN_POINT ( 'NONE',  ( -70.55620429048339304, -23.48783264082478084, -1.443836473390066821 ) ) ;
#94503=CARTESIAN_POINT ( 'NONE',  ( -68.62287095715005592, -29.50250786944525672, 11.44777988621623699 ) ) ;
#94504=CARTESIAN_POINT ( 'NONE',  ( 13.48273455363431772, -16.43370779934446801, -1.500000000000002220 ) ) ;
#94506=CARTESIAN_POINT ( 'NONE',  ( -50.49354941359371196, -24.40034930558990922, 0.3402023900116070698 ) ) ;
#94507=CARTESIAN_POINT ( 'NONE',  ( 16.38291735060997567, -14.39268585342195905, -1.500000000000002220 ) ) ;
#94508=CARTESIAN_POINT ( 'NONE',  ( -103.5550924144477705, -23.96169478059713498, 10.65365249895717881 ) ) ;
#94511=CARTESIAN_POINT ( 'NONE',  ( 13.71991279636371175, 16.93377936151356877, -1.500000000000002220 ) ) ;
#94512=CARTESIAN_POINT ( 'NONE',  ( -66.62287095715005592, -23.47593901973091235, -1.443836447539006196 ) ) ;
#94513=VERTEX_POINT ( 'NONE', #28291 ) ;
#94515=CARTESIAN_POINT ( 'NONE',  ( -85.51038857217308475, -24.15602025860895807, 10.28564288303535967 ) ) ;
#94516=ORIENTED_EDGE ( 'NONE', *, *, #100021, .F. ) ;
#94519=ORIENTED_EDGE ( 'NONE', *, *, #1793, .F. ) ;
#94520=CARTESIAN_POINT ( 'NONE',  ( -28.37442136742509646, -24.86812948212714147, 2.469321321118715495 ) ) ;
#94521=CARTESIAN_POINT ( 'NONE',  ( -82.62360240055558336, -24.65952944569304606, 1.056160979905702790 ) ) ;
#94522=CARTESIAN_POINT ( 'NONE',  ( -6.410030533929251817, 20.24415959294862333, 11.49999999999998934 ) ) ;
#94523=CARTESIAN_POINT ( 'NONE',  ( -94.50573621563975735, -24.65952944569304606, 1.056160979905701680 ) ) ;
#94524=DIRECTION ( 'NONE',  ( -1.000000000000000000, -3.773278334444166432E-23, -8.201307841325785021E-29 ) ) ;
#94525=CARTESIAN_POINT ( 'NONE',  ( -54.52287095715005449, -23.47593901973090169, -1.443836447538997092 ) ) ;
#94526=CARTESIAN_POINT ( 'NONE',  ( -48.55620429048339304, -23.47596703998600276, 11.44779298504227505 ) ) ;
#94528=CARTESIAN_POINT ( 'NONE',  ( 17.66168439605153395, -8.020940556088177686, -1.500000000000002220 ) ) ;
#94530=ORIENTED_EDGE ( 'NONE', *, *, #17952, .F. ) ;
#94531=CARTESIAN_POINT ( 'NONE',  ( 19.32586673001642197, -2.567307930040524599, 11.49999999999999645 ) ) ;
#94535=ORIENTED_EDGE ( 'NONE', *, *, #9007, .F. ) ;
#94536=CARTESIAN_POINT ( 'NONE',  ( -58.62287095715007013, -23.47596703998600276, 11.44779298504227683 ) ) ;
#94537=CARTESIAN_POINT ( 'NONE',  ( -32.55620429048340014, -23.48786465467240347, 11.44779295918255713 ) ) ;
#94538=B_SPLINE_CURVE_WITH_KNOTS ( 'NONE', 3,
 ( #27993, #57964, #73178, #34115, #26502, #20358 ),
 .UNSPECIFIED., .F., .F.,
 ( 4, 2, 4 ),
 ( 0.000000000000000000, 0.001380764517853252070, 0.002761529035706504140 ),
 .UNSPECIFIED. ) ;
#94539=CARTESIAN_POINT ( 'NONE',  ( -103.5228709571501042, -23.47593901973090524, -1.443836447538996204 ) ) ;
#94540=CARTESIAN_POINT ( 'NONE',  ( -93.55798342408773749, -23.73791477778911840, 11.05961554403170410 ) ) ;
#94541=CARTESIAN_POINT ( 'NONE',  ( 6.681059570357060551, -18.48443787736713873, -1.500000000000002220 ) ) ;
#94542=VERTEX_POINT ( 'NONE', #82574 ) ;
#94544=CARTESIAN_POINT ( 'NONE',  ( -114.5562042904833930, -23.47596703998600631, 11.44779298504227683 ) ) ;
#94547=DIRECTION ( 'NONE',  ( 0.000000000000000000, 2.173523156925980399E-06, -0.9999999999976378895 ) ) ;
#94548=CARTESIAN_POINT ( 'NONE',  ( -105.6228709571500275, -25.00182538069145721, 7.747789668545099317 ) ) ;
#94549=CARTESIAN_POINT ( 'NONE',  ( -101.9327573176231283, -25.24367985958541638, 6.326438925865677021 ) ) ;
#94550=EDGE_CURVE ( 'NONE', #20892, #58811, #32792, .T. ) ;
#94551=APPLICATION_CONTEXT ( 'configuration controlled 3d designs of mechanical parts and assemblies' ) ;
#94554=CARTESIAN_POINT ( 'NONE',  ( -114.5149051635414992, -24.66019654487200441, 8.947790411086106843 ) ) ;
#94555=CARTESIAN_POINT ( 'NONE',  ( -18.79874323561663729, 6.599581278811135654, -1.500000000000002220 ) ) ;
#94556=AXIS2_PLACEMENT_3D ( 'NONE', #77525, #38480, #26131 ) ;
#94557=EDGE_CURVE ( 'NONE', #35259, #32133, #13055, .T. ) ;
#94558=CARTESIAN_POINT ( 'NONE',  ( -75.58468866288802701, -24.73531770709095312, 8.716586749053512051 ) ) ;
#94559=CARTESIAN_POINT ( 'NONE',  ( -19.53060160647804722, 3.385818350044136338, -1.500000000000002220 ) ) ;
#94561=CARTESIAN_POINT ( 'NONE',  ( -71.52287095715006160, -23.47593901973090169, -1.443836447538996870 ) ) ;
#94562=EDGE_CURVE ( 'NONE', #46960, #13507, #78905, .T. ) ;
#94565=CARTESIAN_POINT ( 'NONE',  ( -50.67286173397793902, -25.13656437041104752, 7.082003562334411306 ) ) ;
#94567=CARTESIAN_POINT ( 'NONE',  ( -20.69558417703438025, 1.077208295497980250, 11.49999999999999645 ) ) ;
#94568=CARTESIAN_POINT ( 'NONE',  ( -89.81226385320383088, -29.50249917535260380, 7.447779886225679213 ) ) ;
#94569=ADVANCED_FACE ( 'NONE', ( #99772 ), #77444, .T. ) ;
#94570=CARTESIAN_POINT ( 'NONE',  ( -117.6228709571500559, -29.50250243563736774, 8.947779886222134493 ) ) ;
#94571=CARTESIAN_POINT ( 'NONE',  ( -22.70586268970451371, -1.818501321912391999, 11.49999999999999645 ) ) ;
#94572=B_SPLINE_CURVE_WITH_KNOTS ( 'NONE', 3,
 ( #47843, #45843, #38216, #69172 ),
 .UNSPECIFIED., .F., .F.,
 ( 4, 4 ),
 ( 0.000000000000000000, 0.0005192307692307857048 ),
 .UNSPECIFIED. ) ;
#94573=VERTEX_POINT ( 'NONE', #54145 ) ;
#94574=CARTESIAN_POINT ( 'NONE',  ( -69.54934929687469491, -24.15543982623907482, -0.2315651400026648155 ) ) ;
#94575=CARTESIAN_POINT ( 'NONE',  ( -28.52287095715005805, -29.50248298729119867, -6.412432996800796609E-05 ) ) ;
#94576=B_SPLINE_CURVE_WITH_KNOTS ( 'NONE', 3,
 ( #40286, #3244, #64654, #94565, #25048, #17440, #95568, #34178, #65154, #88463, #71240, #25557, #32666, #1727, #48407, #71742 ),
 .UNSPECIFIED., .F., .F.,
 ( 4, 2, 2, 2, 2, 2, 2, 4 ),
 ( 0.000000000000000000, 0.0002012173707785539726, 0.0004024347415571079452, 0.0008048694831142152398, 0.001006086853892760756, 0.001207304224671306271, 0.001408521595449852004, 0.001609738966228397520 ),
 .UNSPECIFIED. ) ;
#94577=VERTEX_POINT ( 'NONE', #30279 ) ;
#94578=CARTESIAN_POINT ( 'NONE',  ( -14.69473627950705108, 13.90061564059656440, -1.500000000000002220 ) ) ;
#94581=CARTESIAN_POINT ( 'NONE',  ( -110.5228709571500758, -24.92604778743018556, 8.074972756849357225 ) ) ;
#94582=ORIENTED_EDGE ( 'NONE', *, *, #72579, .F. ) ;
#94583=DIRECTION ( 'NONE',  ( 3.773278334444167608E-23, -1.000000000000000000, 0.000000000000000000 ) ) ;
#94584=CARTESIAN_POINT ( 'NONE',  ( -9.034649315346676701, 21.08484869742704504, 11.49999999999998934 ) ) ;
#94585=CARTESIAN_POINT ( 'NONE',  ( -35.52287095715006870, -23.47596703998600631, 11.44779298504229281 ) ) ;
#94586=CARTESIAN_POINT ( 'NONE',  ( 14.90458806734895703, -13.33898509196910886, -1.500000000000002220 ) ) ;
#94587=CARTESIAN_POINT ( 'NONE',  ( -41.16195490483097075, -25.07454073646012560, 7.413582391003542327 ) ) ;
#94588=CARTESIAN_POINT ( 'NONE',  ( 19.95448254803897115, -6.385634049875297258, 11.49999999999999645 ) ) ;
#94589=CARTESIAN_POINT ( 'NONE',  ( -28.43316735593882072, -24.74360632443060837, 8.116853411926154394 ) ) ;
#94591=CARTESIAN_POINT ( 'NONE',  ( 22.04941498731238525, 0.3350016526185666255, 11.49999999999998934 ) ) ;
#94592=B_SPLINE_CURVE_WITH_KNOTS ( 'NONE', 3,
 ( #3323, #34253, #65228, #71819 ),
 .UNSPECIFIED., .F., .F.,
 ( 4, 4 ),
 ( 0.000000000000000000, 9.999999999998897304E-05 ),
 .UNSPECIFIED. ) ;
#94593=CARTESIAN_POINT ( 'NONE',  ( -69.52287095715006160, -24.65952944569304606, 1.056160979905697239 ) ) ;
#94596=CARTESIAN_POINT ( 'NONE',  ( -60.52287095715004739, -24.51163499207175178, 0.6490370598554290327 ) ) ;
#94597=CARTESIAN_POINT ( 'NONE',  ( -49.93954932203694597, -25.18440119950784606, 3.376895537457810903 ) ) ;
#94598=CARTESIAN_POINT ( 'NONE',  ( -51.62287095715005592, -24.64898659630367206, 1.056161002820821038 ) ) ;
#94599=EDGE_LOOP ( 'NONE', ( #97573, #50043, #24976, #21213 ) ) ;
#94601=ORIENTED_EDGE ( 'NONE', *, *, #18285, .F. ) ;
#94605=DIRECTION ( 'NONE',  ( -3.773278334444166432E-23, 1.000000000000000000, 0.000000000000000000 ) ) ;
#94606=CARTESIAN_POINT ( 'NONE',  ( -51.52287095715006160, -23.72747288104470087, -1.053458166803227458 ) ) ;
#94607=CARTESIAN_POINT ( 'NONE',  ( 18.14102482237423075, -9.550406459077080967, -1.500000000000002220 ) ) ;
#94608=EDGE_CURVE ( 'NONE', #93091, #38212, #6309, .T. ) ;
#94611=CARTESIAN_POINT ( 'NONE',  ( -33.62287095715007013, -24.35013146730203104, 9.818937971375117257 ) ) ;
#94613=CARTESIAN_POINT ( 'NONE',  ( -22.22805510923732086, 2.117028069546627922, 11.49999999999998934 ) ) ;
#94614=CARTESIAN_POINT ( 'NONE',  ( -71.17271826174675198, -25.19999523107665595, 6.679460637636927878 ) ) ;
#94615=CARTESIAN_POINT ( 'NONE',  ( -25.85053656567609082, -24.78713859579120893, 6.931755823712101083 ) ) ;
#94616=ORIENTED_EDGE ( 'NONE', *, *, #58166, .T. ) ;
#94617=DIRECTION ( 'NONE',  ( 0.000000000000000000, -2.173523156925980399E-06, 0.9999999999976378895 ) ) ;
#94618=CARTESIAN_POINT ( 'NONE',  ( -113.5228709571500616, -23.48786465467242479, 11.44779295918253936 ) ) ;
#94619=CARTESIAN_POINT ( 'NONE',  ( -20.61801493038525379, 2.926015819835423581, 11.49999999999998934 ) ) ;
#94620=ORIENTED_EDGE ( 'NONE', *, *, #88664, .F. ) ;
#94621=CARTESIAN_POINT ( 'NONE',  ( -116.5228709571500474, -23.96127896942151025, -0.6493128930935556653 ) ) ;
#94623=ORIENTED_EDGE ( 'NONE', *, *, #73745, .T. ) ;
#94624=CARTESIAN_POINT ( 'NONE',  ( -69.47374562227740569, -25.03149312170462792, 7.284001176654951948 ) ) ;
#94625=CARTESIAN_POINT ( 'NONE',  ( -6.733481718715807141, 19.98004043397084928, -1.500000000000002220 ) ) ;
#94628=CARTESIAN_POINT ( 'NONE',  ( -93.62287095715012697, -23.96177878511308634, 10.65340807706329507 ) ) ;
#94629=FACE_OUTER_BOUND ( 'NONE', #17099, .T. ) ;
#94630=CARTESIAN_POINT ( 'NONE',  ( -120.5181819260963465, -24.52399227489125266, 9.353111116836528183 ) ) ;
#94631=CARTESIAN_POINT ( 'NONE',  ( -101.9507253916653440, -25.25419265818597125, 6.236250658476948594 ) ) ;
#94632=CARTESIAN_POINT ( 'NONE',  ( -60.62287095715003460, -24.62285846362214770, 9.038163152653524435 ) ) ;
#94633=PLANE ( 'NONE',  #57778 ) ;
#94635=CARTESIAN_POINT ( 'NONE',  ( 4.129723114849880083, -21.82631191821171512, 11.49999999999999645 ) ) ;
#94636=EDGE_LOOP ( 'NONE', ( #16141, #86717, #36824, #74753 ) ) ;
#94637=CARTESIAN_POINT ( 'NONE',  ( -98.89486075440558466, -25.27154821674656660, 6.039256008359274119 ) ) ;
#94638=EDGE_CURVE ( 'NONE', #13615, #45924, #39897, .T. ) ;
#94639=CARTESIAN_POINT ( 'NONE',  ( -70.83100241438432931, -25.29887142613843309, 5.408397035483008430 ) ) ;
#94640=VERTEX_POINT ( 'NONE', #7946 ) ;
#94642=CARTESIAN_POINT ( 'NONE',  ( 17.73637878876437668, -14.10177982315242318, -1.500000000000002220 ) ) ;
#94644=EDGE_LOOP ( 'NONE', ( #29347, #87874, #1485, #18817 ) ) ;
#94645=AXIS2_PLACEMENT_3D ( 'NONE', #62036, #33081, #70137 ) ;
#94646=ORIENTED_EDGE ( 'NONE', *, *, #70085, .F. ) ;
#94649=CARTESIAN_POINT ( 'NONE',  ( -14.30055291515510518, -14.21740073472259525, 11.49999999999998934 ) ) ;
#94650=CARTESIAN_POINT ( 'NONE',  ( -51.52287095715006870, -24.50321055353806443, 9.387540953477529371 ) ) ;
#94652=CARTESIAN_POINT ( 'NONE',  ( -42.62287095715006302, -23.73934037231756378, 11.05740245334329863 ) ) ;
#94653=CARTESIAN_POINT ( 'NONE',  ( -20.28323820415832657, -9.445149539555593776, -1.500000000000002220 ) ) ;
#94654=B_SPLINE_CURVE_WITH_KNOTS ( 'NONE', 3,
 ( #73152, #83627, #3149, #2643, #10747, #33581 ),
 .UNSPECIFIED., .F., .F.,
 ( 4, 2, 4 ),
 ( 6.391158118970788496E-06, 0.001387004593080784845, 0.002767618028042598960 ),
 .UNSPECIFIED. ) ;
#94655=ORIENTED_EDGE ( 'NONE', *, *, #55317, .T. ) ;
#94657=CARTESIAN_POINT ( 'NONE',  ( -112.5891708905303972, -24.35071581493543391, 9.817618358456018157 ) ) ;
#94658=CARTESIAN_POINT ( 'NONE',  ( -119.6228709571500275, -24.33927499327855415, 9.819080762295815390 ) ) ;
#94659=CARTESIAN_POINT ( 'NONE',  ( -110.5895376238167387, -25.00182538069145366, 7.747789668545099317 ) ) ;
#94660=CARTESIAN_POINT ( 'NONE',  ( -41.52287095715005449, -23.48783264083359867, -1.443836473376375329 ) ) ;
#94662=CARTESIAN_POINT ( 'NONE',  ( -0.4769873229303308038, -19.55164744950295841, -1.500000000000002220 ) ) ;
#94663=CARTESIAN_POINT ( 'NONE',  ( -49.64016321101554041, -25.30016906297147017, 4.382939044608830770 ) ) ;
#94664=EDGE_LOOP ( 'NONE', ( #10009, #82218, #86239, #57313 ) ) ;
#94665=CARTESIAN_POINT ( 'NONE',  ( 0.6623178260406717976, 21.47796536025111536, 11.49999999999998934 ) ) ;
#94666=CARTESIAN_POINT ( 'NONE',  ( -128.5562987298943369, -23.48783264082478794, -1.443836473390056829 ) ) ;
#94668=CARTESIAN_POINT ( 'NONE',  ( -101.7379430823953896, -25.25923547149210791, 3.830416064291135569 ) ) ;
#94669=LINE ( 'NONE', #86058, #32596 ) ;
#94670=CARTESIAN_POINT ( 'NONE',  ( 18.56524475492553705, -13.42312393814442650, -1.500000000000002220 ) ) ;
#94673=CARTESIAN_POINT ( 'NONE',  ( -92.62287095715005592, -24.50216790748205753, 0.6166512839542542812 ) ) ;
#94674=CARTESIAN_POINT ( 'NONE',  ( -1.591348192139008466, -19.94584644712825039, 11.49999999999999645 ) ) ;
#94680=CARTESIAN_POINT ( 'NONE',  ( 19.84127317031322946, -0.4231496731191971561, 11.49999999999998934 ) ) ;
#94681=CARTESIAN_POINT ( 'NONE',  ( -19.00758693998263738, -10.61793046214600089, 11.49999999999998934 ) ) ;
#94682=LINE ( 'NONE', #56143, #77136 ) ;
#94683=CARTESIAN_POINT ( 'NONE',  ( 9.442166470422634461, 17.27452087139410963, -1.500000000000002220 ) ) ;
#94685=CARTESIAN_POINT ( 'NONE',  ( -32.52287095715006160, -29.50250786944525672, 11.44777988621624409 ) ) ;
#94687=ADVANCED_FACE ( 'NONE', ( #45527 ), #85568, .F. ) ;
#94688=CARTESIAN_POINT ( 'NONE',  ( -103.5228709571500900, -24.33832256527049154, 0.1851278514138670062 ) ) ;
#94690=CARTESIAN_POINT ( 'NONE',  ( -10.57813111170615983, 17.65445453266677234, 11.49999999999999645 ) ) ;
#94693=B_SPLINE_CURVE_WITH_KNOTS ( 'NONE', 3,
 ( #91160, #84049, #75927, #14026, #19767, #52607 ),
 .UNSPECIFIED., .F., .F.,
 ( 4, 2, 4 ),
 ( 1.570887131794176733E-05, 0.001396322306279758688, 0.002776935741241575838 ),
 .UNSPECIFIED. ) ;
#94694=VECTOR ( 'NONE', #46263, 1000.000000000000114 ) ;
#94695=CARTESIAN_POINT ( 'NONE',  ( -120.5526916197902665, -24.83618233451451118, 1.606449574219542598 ) ) ;
#94696=CARTESIAN_POINT ( 'NONE',  ( 21.71239400539012721, -6.292901409244172406, 11.49999999999999645 ) ) ;
#94697=VERTEX_POINT ( 'NONE', #76446 ) ;
#94698=CARTESIAN_POINT ( 'NONE',  ( -69.78016143783460734, -25.25639569820748065, 6.955938088137161301 ) ) ;
#94699=CARTESIAN_POINT ( 'NONE',  ( -72.52287095715010423, -23.48783264082476308, -1.443836473390092578 ) ) ;
#94701=CARTESIAN_POINT ( 'NONE',  ( -26.99920202386822865, -24.77267274619866910, 2.471679651391708088 ) ) ;
#94702=EDGE_CURVE ( 'NONE', #38526, #63440, #67965, .T. ) ;
#94703=DIRECTION ( 'NONE',  ( -3.773278334444166432E-23, 1.000000000000000000, 0.000000000000000000 ) ) ;
#94704=VECTOR ( 'NONE', #35953, 1000.000000000000114 ) ;
#94705=CARTESIAN_POINT ( 'NONE',  ( -28.52287095715005805, -23.32378116302990279, 11.44779301262222049 ) ) ;
#94706=ORIENTED_EDGE ( 'NONE', *, *, #10457, .F. ) ;
#94707=CARTESIAN_POINT ( 'NONE',  ( 17.26854690438276307, -15.35948741044508559, 11.49999999999999645 ) ) ;
#94708=CARTESIAN_POINT ( 'NONE',  ( 17.70901601935662839, 14.43836031950349152, 11.49999999999998934 ) ) ;
#94710=CARTESIAN_POINT ( 'NONE',  ( -106.6228709571500559, -24.66019654487199730, 8.947790411086122830 ) ) ;
#94711=CARTESIAN_POINT ( 'NONE',  ( -82.54134713839933113, -24.66019654487199730, 8.947790411086122830 ) ) ;
#94712=CARTESIAN_POINT ( 'NONE',  ( 12.95044643391442030, 18.39415735498938176, 11.49999999999999645 ) ) ;
#94714=CARTESIAN_POINT ( 'NONE',  ( -30.57287095715006231, -29.50250786944500803, 11.44777977285526838 ) ) ;
#94715=CARTESIAN_POINT ( 'NONE',  ( -8.471812324360341151, -20.26817064352238162, -1.500000000000002220 ) ) ;
#94716=CARTESIAN_POINT ( 'NONE',  ( -82.52287095715006160, -29.50248528299804818, 1.056150453629038477 ) ) ;
#94717=CARTESIAN_POINT ( 'NONE',  ( -44.53462723111864818, -24.51419770103159479, 9.386484678747171628 ) ) ;
#94718=CARTESIAN_POINT ( 'NONE',  ( -61.52287095715006160, -24.66019654487199730, 8.947790411086121054 ) ) ;
#94719=ORIENTED_EDGE ( 'NONE', *, *, #19862, .T. ) ;
#94722=EDGE_LOOP ( 'NONE', ( #22779, #41200, #79242, #97983 ) ) ;
#94723=CARTESIAN_POINT ( 'NONE',  ( -1.317410511717131971, -20.46822056820986546, -1.500000000000002220 ) ) ;
#94724=ORIENTED_EDGE ( 'NONE', *, *, #82823, .F. ) ;
#94725=ORIENTED_EDGE ( 'NONE', *, *, #97562, .F. ) ;
#94726=VERTEX_POINT ( 'NONE', #92180 ) ;
#94728=CARTESIAN_POINT ( 'NONE',  ( 11.81885653190370888, -19.86314957129924608, -1.500000000000002220 ) ) ;
#94730=CARTESIAN_POINT ( 'NONE',  ( -5.191926799570463658, 19.71030214607805675, -1.500000000000002220 ) ) ;
#94731=ORIENTED_EDGE ( 'NONE', *, *, #90686, .F. ) ;
#94733=FACE_OUTER_BOUND ( 'NONE', #17739, .T. ) ;
#94734=EDGE_CURVE ( 'NONE', #94858, #55468, #46515, .T. ) ;
#94735=FACE_OUTER_BOUND ( 'NONE', #43027, .T. ) ;
#94737=CARTESIAN_POINT ( 'NONE',  ( -12.84383942963603964, -17.20202612561282862, 11.49999999999999645 ) ) ;
#94738=ORIENTED_EDGE ( 'NONE', *, *, #4338, .T. ) ;
#94739=CARTESIAN_POINT ( 'NONE',  ( -75.58469511993916967, -24.73486907724918282, 1.287355809206967683 ) ) ;
#94740=LINE ( 'NONE', #96252, #11840 ) ;
#94743=CARTESIAN_POINT ( 'NONE',  ( -11.67826063220891086, 17.12864047899337550, -1.500000000000002220 ) ) ;
#94745=EDGE_CURVE ( 'NONE', #22830, #61303, #37756, .T. ) ;
#94746=CARTESIAN_POINT ( 'NONE',  ( -71.62287095715005592, -23.48783264082478084, -1.443836473390067487 ) ) ;
#94747=ORIENTED_EDGE ( 'NONE', *, *, #50704, .F. ) ;
#94750=EDGE_LOOP ( 'NONE', ( #11395, #68174, #93856, #38793 ) ) ;
#94752=CARTESIAN_POINT ( 'NONE',  ( -40.52287095715006160, -24.63287334234178161, 0.9662140553045331925 ) ) ;
#94753=CARTESIAN_POINT ( 'NONE',  ( -42.56072409594817429, -23.73791477778911485, 11.05961554403171299 ) ) ;
#94754=CARTESIAN_POINT ( 'NONE',  ( -43.62370922560796060, -24.66019654487199375, 8.947790411086121054 ) ) ;
#94755=CARTESIAN_POINT ( 'NONE',  ( 16.16784302627978320, -14.93143893958281154, 11.49999999999999645 ) ) ;
#94757=CARTESIAN_POINT ( 'NONE',  ( -47.62287095715005592, -23.96177878511308634, 10.65340807706330217 ) ) ;
#94758=CARTESIAN_POINT ( 'NONE',  ( -16.68516988606489448, 15.22057433622007316, 11.49999999999998934 ) ) ;
#94759=CARTESIAN_POINT ( 'NONE',  ( 19.96068868648078620, -6.529529906025321573, 11.49999999999998934 ) ) ;
#94760=CARTESIAN_POINT ( 'NONE',  ( -30.49303573129054357, -23.47596703998576118, 11.44779287168131710 ) ) ;
#94762=ORIENTED_EDGE ( 'NONE', *, *, #89441, .F. ) ;
#94766=B_SPLINE_CURVE_WITH_KNOTS ( 'NONE', 3,
 ( #63568, #25477, #3164, #34105 ),
 .UNSPECIFIED., .F., .F.,
 ( 4, 4 ),
 ( 0.000000000000000000, 0.0001000000000000028644 ),
 .UNSPECIFIED. ) ;
#94767=CARTESIAN_POINT ( 'NONE',  ( -57.58746848899791360, -24.35071581493543036, 9.817618358456028815 ) ) ;
#94769=CARTESIAN_POINT ( 'NONE',  ( 12.34367313097222763, -17.18290682204727915, 11.49999999999998934 ) ) ;
#94771=CARTESIAN_POINT ( 'NONE',  ( -60.73340568811573803, -25.03722704563418944, 7.590184509431679771 ) ) ;
#94772=CARTESIAN_POINT ( 'NONE',  ( -75.62287095715004170, -23.84047902841601640, -0.8780736468305718745 ) ) ;
#94774=CARTESIAN_POINT ( 'NONE',  ( -101.5228709571500048, -23.73907113216990084, -1.053371485793246354 ) ) ;
#94775=CARTESIAN_POINT ( 'NONE',  ( -21.14947813473477822, 6.846651710974520633, -1.500000000000002220 ) ) ;
#94776=CARTESIAN_POINT ( 'NONE',  ( -114.5916530783749323, -23.96119346886881729, -0.6495511937831860427 ) ) ;
#94777=VECTOR ( 'NONE', #10636, 1000.000000000000114 ) ;
#94778=VERTEX_POINT ( 'NONE', #64775 ) ;
#94781=CARTESIAN_POINT ( 'NONE',  ( -126.5222601566329530, -23.48783264082477018, -1.443836473390087249 ) ) ;
#94783=CARTESIAN_POINT ( 'NONE',  ( -71.62287095715005592, -23.48783264082478084, -1.443836473390067487 ) ) ;
#94785=CARTESIAN_POINT ( 'NONE',  ( 1.793504005174451077, 19.40006364325761012, -1.500000000000002220 ) ) ;
#94786=CARTESIAN_POINT ( 'NONE',  ( -21.12015818079280649, -3.594773940630530795, -1.500000000000002220 ) ) ;
#94788=CARTESIAN_POINT ( 'NONE',  ( -60.63370354675536333, -24.63419186845290199, 9.035850630957110496 ) ) ;
#94789=DIRECTION ( 'NONE',  ( 0.000000000000000000, -0.8406134417706495610, -0.5416355246053408123 ) ) ;
#94790=CARTESIAN_POINT ( 'NONE',  ( -77.49793897276390453, -24.65952944569304606, 1.056160979905701458 ) ) ;
#94791=CARTESIAN_POINT ( 'NONE',  ( 2.440706796964721370, 22.61111150098722788, -1.500000000000002220 ) ) ;
#94793=CARTESIAN_POINT ( 'NONE',  ( -102.5930987670637791, -23.96119346886881729, -0.6495511937831878191 ) ) ;
#94794=CARTESIAN_POINT ( 'NONE',  ( -80.52287095715006160, -24.99132157543083821, 2.256160258750667502 ) ) ;
#94795=CARTESIAN_POINT ( 'NONE',  ( -0.3680779360730609406, 19.82951397037014729, 11.49999999999999645 ) ) ;
#94799=CARTESIAN_POINT ( 'NONE',  ( -51.52287095715008292, -23.47593901973090169, -1.443836447538997092 ) ) ;
#94800=ADVANCED_FACE ( 'NONE', ( #48024 ), #41922, .F. ) ;
#94802=DIRECTION ( 'NONE',  ( -0.000000000000000000, 2.173523156925979552E-06, -0.9999999999976378895 ) ) ;
#94804=CARTESIAN_POINT ( 'NONE',  ( -75.58953762381673869, -24.99132157543084176, 2.256160258750496084 ) ) ;
#94805=CARTESIAN_POINT ( 'NONE',  ( -21.46818342838279392, -2.986162219498790904, -1.500000000000002220 ) ) ;
#94807=CARTESIAN_POINT ( 'NONE',  ( 10.93668938013857783, -16.14717738681254033, -1.500000000000002220 ) ) ;
#94808=CARTESIAN_POINT ( 'NONE',  ( -123.6228709571500559, -24.66019654487200086, 8.947790411086117501 ) ) ;
#94809=ORIENTED_EDGE ( 'NONE', *, *, #47177, .T. ) ;
#94811=B_SPLINE_CURVE_WITH_KNOTS ( 'NONE', 3,
 ( #24467, #85873, #40702, #17359, #71655, #2155, #64067, #95486 ),
 .UNSPECIFIED., .F., .F.,
 ( 4, 2, 2, 4 ),
 ( -0.001240666984355833034, -0.0002401179793394905577, 0.0007604310256768519183, 0.002761529035709536003 ),
 .UNSPECIFIED. ) ;
#94812=CARTESIAN_POINT ( 'NONE',  ( -1.067026067711715154, -20.38227831319515460, 11.49999999999999645 ) ) ;
#94817=ORIENTED_EDGE ( 'NONE', *, *, #24180, .T. ) ;
#94818=CARTESIAN_POINT ( 'NONE',  ( -80.51244414166535535, -25.03284467579916495, 7.563174216508125269 ) ) ;
#94820=CARTESIAN_POINT ( 'NONE',  ( -75.55620429048340725, -23.47596703998600276, 11.44779298504227683 ) ) ;
#94823=EDGE_CURVE ( 'NONE', #13993, #18934, #50031, .T. ) ;
#94824=CARTESIAN_POINT ( 'NONE',  ( -109.5961215800431745, -23.48783264082476663, -1.443836473390089470 ) ) ;
#94826=FACE_OUTER_BOUND ( 'NONE', #7878, .T. ) ;
#94827=EDGE_CURVE ( 'NONE', #7414, #95483, #74074, .T. ) ;
#94828=CARTESIAN_POINT ( 'NONE',  ( -22.24355531667433539, 5.575215412481045796, 11.49999999999999645 ) ) ;
#94829=CARTESIAN_POINT ( 'NONE',  ( -4.508144621425604903, 22.28865971958312997, 11.49999999999998934 ) ) ;
#94831=CARTESIAN_POINT ( 'NONE',  ( -110.5109840011334086, -24.92592662359561473, 8.075495903018000021 ) ) ;
#94832=CARTESIAN_POINT ( 'NONE',  ( -48.52287095715006160, -24.64898659630367561, 1.056161002820821038 ) ) ;
#94833=CARTESIAN_POINT ( 'NONE',  ( -90.50790128547902214, -24.40034930558990922, 0.3402023900116079580 ) ) ;
#94834=DIRECTION ( 'NONE',  ( -3.773278334453079618E-23, 0.9999999999976377785, 2.173523156925979975E-06 ) ) ;
#94835=AXIS2_PLACEMENT_3D ( 'NONE', #28941, #75596, #36547 ) ;
#94837=CARTESIAN_POINT ( 'NONE',  ( -27.32356460660396635, -24.75521138200594251, 2.326351302823062461 ) ) ;
#94838=CARTESIAN_POINT ( 'NONE',  ( -122.5201565697420705, -24.15543982623907482, -0.2315651400026565998 ) ) ;
#94839=CARTESIAN_POINT ( 'NONE',  ( -39.62287095715005592, -23.47593901973091235, -1.443836447539011525 ) ) ;
#94840=ORIENTED_EDGE ( 'NONE', *, *, #12786, .T. ) ;
#94841=CARTESIAN_POINT ( 'NONE',  ( -18.82316870354832616, 7.800066519331792847, -1.500000000000002220 ) ) ;
#94844=CARTESIAN_POINT ( 'NONE',  ( 21.12055942831636202, -9.126644407798330860, -1.500000000000002220 ) ) ;
#94847=ORIENTED_EDGE ( 'NONE', *, *, #41434, .T. ) ;
#94851=CARTESIAN_POINT ( 'NONE',  ( -95.64416171314925919, -23.48783264082477373, -1.443836473390088804 ) ) ;
#94853=CARTESIAN_POINT ( 'NONE',  ( -21.15786647118399699, 2.672229404501205163, 11.49999999999999645 ) ) ;
#94855=ORIENTED_EDGE ( 'NONE', *, *, #13227, .T. ) ;
#94856=CARTESIAN_POINT ( 'NONE',  ( -2.380169663812839342, 22.11153957539610104, 11.49999999999998934 ) ) ;
#94857=CARTESIAN_POINT ( 'NONE',  ( 9.220172233967117492, 18.46515239161685784, 11.49999999999998934 ) ) ;
#94858=VERTEX_POINT ( 'NONE', #2352 ) ;
#94860=PLANE ( 'NONE',  #918 ) ;
#94862=CARTESIAN_POINT ( 'NONE',  ( -68.92598737797662523, -25.11539253604531297, 2.804427796191110378 ) ) ;
#94863=ORIENTED_EDGE ( 'NONE', *, *, #81750, .T. ) ;
#94864=CARTESIAN_POINT ( 'NONE',  ( -65.52287095715006160, -25.00158670708909625, 2.256160236439166411 ) ) ;
#94866=CARTESIAN_POINT ( 'NONE',  ( -56.52287095715006870, -24.64965694238407323, 8.947790433994201820 ) ) ;
#94867=CARTESIAN_POINT ( 'NONE',  ( -6.911038104174170194, -19.68591361114308214, -1.500000000000002220 ) ) ;
#94868=CARTESIAN_POINT ( 'NONE',  ( 13.92123049006271707, -16.85212209846622855, 11.49999999999999645 ) ) ;
#94869=CARTESIAN_POINT ( 'NONE',  ( -26.50032570333037185, -24.77993642618010739, 6.891654967618674021 ) ) ;
#94870=PLANE ( 'NONE',  #4602 ) ;
#94871=CARTESIAN_POINT ( 'NONE',  ( -5.125883829288005344, 21.89707322345674712, -1.500000000000002220 ) ) ;
#94872=CARTESIAN_POINT ( 'NONE',  ( -26.31589504439661198, -24.97067121658517763, 6.467908153096676216 ) ) ;
#94875=ORIENTED_EDGE ( 'NONE', *, *, #59997, .F. ) ;
#94876=VECTOR ( 'NONE', #83708, 1000.000000000000114 ) ;
#94877=VERTEX_POINT ( 'NONE', #88087 ) ;
#94878=EDGE_LOOP ( 'NONE', ( #75236, #65432, #30094, #56461 ) ) ;
#94879=CARTESIAN_POINT ( 'NONE',  ( -52.65920731591500470, -23.48783264082478439, -1.443836473390069708 ) ) ;
#94880=EDGE_LOOP ( 'NONE', ( #28616, #41741, #65359, #7724 ) ) ;
#94881=B_SPLINE_CURVE_WITH_KNOTS ( 'NONE', 3,
 ( #23583, #70779, #54553, #15974, #32204, #46944 ),
 .UNSPECIFIED., .F., .F.,
 ( 4, 2, 4 ),
 ( 0.000000000000000000, 0.001380764517854764966, 0.002761529035709529931 ),
 .UNSPECIFIED. ) ;
#94883=CARTESIAN_POINT ( 'NONE',  ( -16.30254408640404051, -13.89340296626662230, -1.500000000000002220 ) ) ;
#94884=CARTESIAN_POINT ( 'NONE',  ( -18.94483701893047467, 11.91932228829616669, 11.49999999999999645 ) ) ;
#94885=VERTEX_POINT ( 'NONE', #32786 ) ;
#94887=CARTESIAN_POINT ( 'NONE',  ( 20.15827220212406701, 6.050813824765241655, 11.49999999999998934 ) ) ;
#94888=CARTESIAN_POINT ( 'NONE',  ( -30.56645522924517167, -24.05349334839690556, 10.47557002954947336 ) ) ;
#94889=CARTESIAN_POINT ( 'NONE',  ( -19.91179686852411734, 0.6080443046932394457, -1.500000000000002220 ) ) ;
#94890=CARTESIAN_POINT ( 'NONE',  ( -127.5228709571500616, -29.50247984919015209, -1.443849546365044922 ) ) ;
#94892=EDGE_CURVE ( 'NONE', #9907, #72214, #94682, .T. ) ;
#94893=CARTESIAN_POINT ( 'NONE',  ( 10.81757466760856801, -19.22619917341675588, -1.500000000000002220 ) ) ;
#94894=ORIENTED_EDGE ( 'NONE', *, *, #55288, .F. ) ;
#94895=CARTESIAN_POINT ( 'NONE',  ( -116.6262420726256153, -24.15543982623908548, -0.2315651400026406959 ) ) ;
#94897=DIRECTION ( 'NONE',  ( 0.000000000000000000, 2.173523156925980399E-06, -0.9999999999976378895 ) ) ;
#94898=CARTESIAN_POINT ( 'NONE',  ( 20.34438994040483806, -4.565235006643893811, 11.49999999999999645 ) ) ;
#94900=EDGE_CURVE ( 'NONE', #58571, #38564, #92200, .T. ) ;
#94902=CARTESIAN_POINT ( 'NONE',  ( -125.5228709571501184, -23.84081130425357742, 10.88220057483160019 ) ) ;
#94903=ADVANCED_FACE ( 'NONE', ( #5832 ), #28674, .T. ) ;
#94905=CARTESIAN_POINT ( 'NONE',  ( -21.15786647118399699, 2.672229404501205163, 11.49999999999998934 ) ) ;
#94906=CARTESIAN_POINT ( 'NONE',  ( -97.62287095715009855, -23.73934037231757443, 11.05740245334328797 ) ) ;
#94910=CARTESIAN_POINT ( 'NONE',  ( 11.79716412695777272, 19.27136520130675024, -1.500000000000002220 ) ) ;
#94913=ORIENTED_EDGE ( 'NONE', *, *, #86238, .T. ) ;
#94914=AXIS2_PLACEMENT_3D ( 'NONE', #28996, #21370, #52344 ) ;
#94915=CARTESIAN_POINT ( 'NONE',  ( -35.62287095715007013, -23.85229601348995843, 10.88205029486209696 ) ) ;
#94916=CARTESIAN_POINT ( 'NONE',  ( -31.65923204074635322, -23.73791477778911130, 11.05961554403171299 ) ) ;
#94917=CARTESIAN_POINT ( 'NONE',  ( 17.66836560233463516, 8.693963128369697202, 11.49999999999999645 ) ) ;
#94918=CARTESIAN_POINT ( 'NONE',  ( -40.92287095715006728, -23.47593901973090169, -1.443836447538997980 ) ) ;
#94919=CARTESIAN_POINT ( 'NONE',  ( -119.5228709571500758, -23.95044443724993144, 10.65354141964648882 ) ) ;
#94921=EDGE_CURVE ( 'NONE', #80400, #79347, #69205, .T. ) ;
#94924=CARTESIAN_POINT ( 'NONE',  ( -99.55766089306172262, -23.73766607897671577, -1.055555164236429366 ) ) ;
#94926=CARTESIAN_POINT ( 'NONE',  ( -124.6228709571500559, -24.64898659630368627, 1.056161002820833028 ) ) ;
#94927=PLANE ( 'NONE',  #21008 ) ;
#94930=B_SPLINE_CURVE_WITH_KNOTS ( 'NONE', 3,
 ( #2818, #4809, #18524, #33758, #35761, #11418, #34757, #4313 ),
 .UNSPECIFIED., .F., .F.,
 ( 4, 2, 2, 4 ),
 ( -0.001240666984355850598, -0.0002401179793395079049, 0.0007604310256768347879, 0.002761529035709519957 ),
 .UNSPECIFIED. ) ;
#94932=CARTESIAN_POINT ( 'NONE',  ( 16.04393857186779115, -11.51807295290239885, -1.500000000000002220 ) ) ;
#94933=ORIENTED_EDGE ( 'NONE', *, *, #18090, .T. ) ;
#94934=CARTESIAN_POINT ( 'NONE',  ( -6.993686169601437186, 18.98418669460116348, 11.49999999999999645 ) ) ;
#94937=EDGE_CURVE ( 'NONE', #24503, #62807, #92090, .T. ) ;
#94940=CARTESIAN_POINT ( 'NONE',  ( -72.55620429048340725, -23.47596703998600276, 11.44779298504227683 ) ) ;
#94941=CARTESIAN_POINT ( 'NONE',  ( -100.4498239493576648, -25.03145178868323129, 7.563174219535599541 ) ) ;
#94943=PLANE ( 'NONE',  #57083 ) ;
#94945=CARTESIAN_POINT ( 'NONE',  ( -17.62595516807937557, -9.487554784798948759, 11.49999999999998934 ) ) ;
#94946=ADVANCED_FACE ( 'NONE', ( #12936 ), #68821, .T. ) ;
#94947=CARTESIAN_POINT ( 'NONE',  ( -58.62287095715004881, -24.64898659630367916, 1.056161002820822592 ) ) ;
#94948=CARTESIAN_POINT ( 'NONE',  ( -116.5926300250966250, -23.73791477778912551, 11.05961554403170055 ) ) ;
#94949=VERTEX_POINT ( 'NONE', #58632 ) ;
#94952=CARTESIAN_POINT ( 'NONE',  ( -104.6228709571500559, -24.35013146730204170, 9.818937971375104823 ) ) ;
#94953=CARTESIAN_POINT ( 'NONE',  ( -35.53623699164313621, -24.52300882791529446, 0.6510814631126419227 ) ) ;
#94955=DIRECTION ( 'NONE',  ( 0.000000000000000000, -2.173523156925980399E-06, 0.9999999999976378895 ) ) ;
#94956=CARTESIAN_POINT ( 'NONE',  ( -73.62362702054829811, -24.65952944569304606, 1.056160979905700126 ) ) ;
#94958=EDGE_CURVE ( 'NONE', #26695, #21027, #44410, .T. ) ;
#94959=CARTESIAN_POINT ( 'NONE',  ( -73.62287095715009855, -24.34917612406837861, 0.1852690917426641770 ) ) ;
#94960=VERTEX_POINT ( 'NONE', #98669 ) ;
#94961=CARTESIAN_POINT ( 'NONE',  ( -6.898722100468609675, -19.10483383855023476, 11.49999999999998934 ) ) ;
#94962=FACE_OUTER_BOUND ( 'NONE', #79248, .T. ) ;
#94963=CARTESIAN_POINT ( 'NONE',  ( -127.5556650442294995, -24.15620529776629155, 10.23563542870658694 ) ) ;
#94964=CARTESIAN_POINT ( 'NONE',  ( -107.5228709571501042, -24.66019654487199730, 8.947790411086115725 ) ) ;
#94965=VECTOR ( 'NONE', #9130, 1000.000000000000114 ) ;
#94967=CARTESIAN_POINT ( 'NONE',  ( -15.68702345270385834, -14.21367052863537417, 11.49999999999999645 ) ) ;
#94968=CARTESIAN_POINT ( 'NONE',  ( -21.57569705560537088, 4.917917830663471435, -1.500000000000002220 ) ) ;
#94969=CARTESIAN_POINT ( 'NONE',  ( -18.72588118538106272, -8.511115862834014223, -1.500000000000002220 ) ) ;
#94974=CARTESIAN_POINT ( 'NONE',  ( -54.57824925133036942, -24.65952944569304606, 1.056160979905696573 ) ) ;
#94975=CARTESIAN_POINT ( 'NONE',  ( -74.62287095715005592, -29.50248528299804818, 1.056150453629036701 ) ) ;
#94976=ORIENTED_EDGE ( 'NONE', *, *, #44196, .F. ) ;
#94981=DIRECTION ( 'NONE',  ( 0.000000000000000000, 2.173523156925980399E-06, -0.9999999999976378895 ) ) ;
#94984=CARTESIAN_POINT ( 'NONE',  ( 7.508984785159893427, -19.29828013722326929, -1.500000000000002220 ) ) ;
#94986=CARTESIAN_POINT ( 'NONE',  ( -21.63489631200954122, -1.325961216813365429, 11.49999999999999645 ) ) ;
#94989=CARTESIAN_POINT ( 'NONE',  ( -110.4124944177896168, -25.11072899458616803, 2.834579673487489959 ) ) ;
#94990=CARTESIAN_POINT ( 'NONE',  ( 22.37589550080693712, 1.095942408959037273, 11.49999999999998934 ) ) ;
#94991=CARTESIAN_POINT ( 'NONE',  ( -47.65344956067661997, -23.73791477778911485, 11.05961554403170766 ) ) ;
#94992=CARTESIAN_POINT ( 'NONE',  ( -61.52287095715006160, -24.64965694238407323, 8.947790433994201820 ) ) ;
#94993=ORIENTED_EDGE ( 'NONE', *, *, #32591, .T. ) ;
#94997=B_SPLINE_CURVE_WITH_KNOTS ( 'NONE', 3,
 ( #73384, #96703, #21070, #44431 ),
 .UNSPECIFIED., .F., .F.,
 ( 4, 4 ),
 ( 0.6792605734346469637, 0.6802613204754125453 ),
 .UNSPECIFIED. ) ;
#94998=ORIENTED_EDGE ( 'NONE', *, *, #34804, .F. ) ;
#94999=CARTESIAN_POINT ( 'NONE',  ( -70.92287095715008149, -23.47596703998600631, 11.44779298504227683 ) ) ;
#95000=VERTEX_POINT ( 'NONE', #62628 ) ;
#95001=CARTESIAN_POINT ( 'NONE',  ( -101.5228709571500758, -23.47596703998600631, 11.44779298504228215 ) ) ;
#95003=CARTESIAN_POINT ( 'NONE',  ( 20.49604761983493972, 5.601127818285958071, -1.500000000000002220 ) ) ;
#95004=B_SPLINE_CURVE_WITH_KNOTS ( 'NONE', 3,
 ( #76886, #53093, #37364, #54092, #24115, #61210, #22111, #99725 ),
 .UNSPECIFIED., .F., .F.,
 ( 4, 2, 2, 4 ),
 ( -0.001224554619866354303, -0.0002241820295893731229, 0.0007761905606876080572, 0.002776935741241574537 ),
 .UNSPECIFIED. ) ;
#95005=ORIENTED_EDGE ( 'NONE', *, *, #55442, .F. ) ;
#95006=CARTESIAN_POINT ( 'NONE',  ( -50.47721621591080066, -24.92564183028979130, 1.928384488918255535 ) ) ;
#95007=EDGE_CURVE ( 'NONE', #15801, #45491, #24446, .T. ) ;
#95008=CARTESIAN_POINT ( 'NONE',  ( -19.11951126197014261, -10.51958540666066533, 11.49999999999998934 ) ) ;
#95009=CARTESIAN_POINT ( 'NONE',  ( -103.5510008564771454, -24.35071581493543391, 9.817618358456027039 ) ) ;
#95010=CARTESIAN_POINT ( 'NONE',  ( -107.5228709571501042, -23.47593901973090524, -1.443836447538996426 ) ) ;
#95011=DIRECTION ( 'NONE',  ( 0.000000000000000000, -2.173523156925980399E-06, 0.9999999999976378895 ) ) ;
#95012=CARTESIAN_POINT ( 'NONE',  ( 3.337383349182757364, -21.60657791699550856, -1.500000000000002220 ) ) ;
#95013=CARTESIAN_POINT ( 'NONE',  ( -30.57287095715005165, -24.38734503390291053, 9.674897050867153681 ) ) ;
#95014=ORIENTED_EDGE ( 'NONE', *, *, #1690, .F. ) ;
#95015=FACE_OUTER_BOUND ( 'NONE', #70048, .T. ) ;
#95016=CARTESIAN_POINT ( 'NONE',  ( -85.54661622668413656, -24.52399227489127043, 9.353111116836526406 ) ) ;
#95017=ORIENTED_EDGE ( 'NONE', *, *, #42140, .T. ) ;
#95018=EDGE_CURVE ( 'NONE', #21576, #54707, #3813, .T. ) ;
#95022=EDGE_CURVE ( 'NONE', #46454, #38937, #14637, .T. ) ;
#95023=EDGE_LOOP ( 'NONE', ( #13500, #12351, #89051, #49618 ) ) ;
#95024=CARTESIAN_POINT ( 'NONE',  ( -89.43576144935767047, -25.12049752546737835, 2.832404795212221771 ) ) ;
#95026=CARTESIAN_POINT ( 'NONE',  ( -82.59968302428518427, -23.73766607897671221, -1.055555164236435362 ) ) ;
#95027=CARTESIAN_POINT ( 'NONE',  ( 18.67678363807796416, 10.12720680154768971, -1.500000000000002220 ) ) ;
#95028=FACE_OUTER_BOUND ( 'NONE', #62294, .T. ) ;
#95029=CARTESIAN_POINT ( 'NONE',  ( -30.59800378598952264, -24.75991027412949563, 1.063373454495736725 ) ) ;
#95032=CARTESIAN_POINT ( 'NONE',  ( 7.147005326088517130, -18.03964237587283037, -1.500000000000002220 ) ) ;
#95033=CARTESIAN_POINT ( 'NONE',  ( -45.62627816233564459, -24.92564183028979130, 1.928384488918256645 ) ) ;
#95035=CARTESIAN_POINT ( 'NONE',  ( 16.17817332762582794, -10.88531698672339942, 11.49999999999999645 ) ) ;
#95044=LINE ( 'NONE', #10310, #70414 ) ;
#95045=CARTESIAN_POINT ( 'NONE',  ( 9.421224358276909072, -17.24829524558457194, 11.49999999999998934 ) ) ;
#95047=B_SPLINE_CURVE_WITH_KNOTS ( 'NONE', 3,
 ( #65342, #57707, #19121, #97252, #79526, #41473 ),
 .UNSPECIFIED., .F., .F.,
 ( 4, 2, 4 ),
 ( 0.000000000000000000, 0.001380764517853253371, 0.002761529035706506742 ),
 .UNSPECIFIED. ) ;
#95048=ORIENTED_EDGE ( 'NONE', *, *, #8693, .T. ) ;
#95049=PLANE ( 'NONE',  #22923 ) ;
#95050=CARTESIAN_POINT ( 'NONE',  ( -22.22199965279648737, -6.226755796435518242, -1.500000000000002220 ) ) ;
#95051=AXIS2_PLACEMENT_3D ( 'NONE', #62513, #1111, #64040 ) ;
#95052=B_SPLINE_CURVE_WITH_KNOTS ( 'NONE', 3,
 ( #82256, #51822, #35600, #44208 ),
 .UNSPECIFIED., .F., .F.,
 ( 4, 4 ),
 ( 0.000000000000000000, 9.999999999998897304E-05 ),
 .UNSPECIFIED. ) ;
#95054=DIRECTION ( 'NONE',  ( 0.000000000000000000, -2.173523156925980399E-06, 0.9999999999976378895 ) ) ;
#95055=CARTESIAN_POINT ( 'NONE',  ( -105.6228709571501128, -24.62285846362216191, 9.038163152653526211 ) ) ;
#95056=CARTESIAN_POINT ( 'NONE',  ( -110.2249299094570034, -25.11071250048269121, 2.834488755612520894 ) ) ;
#95057=CARTESIAN_POINT ( 'NONE',  ( -29.52287095715006160, -23.38909342368989641, 11.44779306042727285 ) ) ;
#95058=CARTESIAN_POINT ( 'NONE',  ( -79.91736924226242422, -25.29489613318244068, 6.057562805997258160 ) ) ;
#95062=FACE_OUTER_BOUND ( 'NONE', #7871, .T. ) ;
#95065=CARTESIAN_POINT ( 'NONE',  ( -19.25010300378637851, 5.133817055790010464, 11.49999999999998934 ) ) ;
#95066=CARTESIAN_POINT ( 'NONE',  ( -100.5388770704638546, -25.19555990040513294, 3.297675640329406743 ) ) ;
#95067=CARTESIAN_POINT ( 'NONE',  ( 12.34629653512297409, 15.52844579862587437, -1.500000000000002220 ) ) ;
#95070=CARTESIAN_POINT ( 'NONE',  ( -77.62287095715005592, -29.50248528299804818, 1.056150453629038477 ) ) ;
#95071=ADVANCED_FACE ( 'NONE', ( #84447 ), #38271, .T. ) ;
#95072=CARTESIAN_POINT ( 'NONE',  ( -104.6228709571500559, -24.64965695001468404, 8.947790433994178727 ) ) ;
#95074=CARTESIAN_POINT ( 'NONE',  ( 20.75994597877129877, -1.272245555857973054, 11.49999999999999645 ) ) ;
#95075=CARTESIAN_POINT ( 'NONE',  ( -81.56339547467169382, -23.48783264082478084, -1.443836473390067043 ) ) ;
#95078=CARTESIAN_POINT ( 'NONE',  ( 10.87194125936840194, 20.03610521102953257, 11.49999999999999645 ) ) ;
#95080=CARTESIAN_POINT ( 'NONE',  ( -111.9228709571500815, -23.47596703998600631, 11.44779298504227860 ) ) ;
#95081=FACE_OUTER_BOUND ( 'NONE', #44467, .T. ) ;
#95083=CARTESIAN_POINT ( 'NONE',  ( -18.82339984186270598, 7.397194320553815317, 11.49999999999998934 ) ) ;
#95085=CARTESIAN_POINT ( 'NONE',  ( -49.58953762381673158, -24.65952944569304606, 1.056160979905694575 ) ) ;
#95087=CARTESIAN_POINT ( 'NONE',  ( -106.6228709571500559, -24.64898659630368627, 1.056161002820831474 ) ) ;
#95088=VERTEX_POINT ( 'NONE', #77815 ) ;
#95089=CARTESIAN_POINT ( 'NONE',  ( -127.5228709571500900, -24.51283580621365843, 0.6167428607019854736 ) ) ;
#95090=CARTESIAN_POINT ( 'NONE',  ( -100.6228709571500843, -23.84047902841604483, -0.8780736468305493370 ) ) ;
#95091=CARTESIAN_POINT ( 'NONE',  ( -12.65591448191638335, 15.52279176289047236, -1.500000000000002220 ) ) ;
#95092=CARTESIAN_POINT ( 'NONE',  ( -36.62287095715007723, -24.33927499327853639, 9.819080762295818943 ) ) ;
#95093=CARTESIAN_POINT ( 'NONE',  ( -18.84683179826791743, -9.195131953753229226, 11.49999999999999645 ) ) ;
#95097=CARTESIAN_POINT ( 'NONE',  ( 13.08019894233326319, 17.74467248152726384, -1.500000000000002220 ) ) ;
#95101=FACE_OUTER_BOUND ( 'NONE', #12984, .T. ) ;
#95102=CARTESIAN_POINT ( 'NONE',  ( -72.49564566603571336, -24.65952944569304250, 1.056160979905695463 ) ) ;
#95103=VERTEX_POINT ( 'NONE', #39270 ) ;
#95105=ORIENTED_EDGE ( 'NONE', *, *, #62977, .T. ) ;
#95107=PLANE ( 'NONE',  #19470 ) ;
#95108=CARTESIAN_POINT ( 'NONE',  ( -100.5578068411443837, -25.10935802950346130, 2.834635647046928941 ) ) ;
#95110=CARTESIAN_POINT ( 'NONE',  ( -10.27258457790969892, -17.75692283049141196, -1.500000000000002220 ) ) ;
#95114=CARTESIAN_POINT ( 'NONE',  ( -41.52287095715006870, -24.64965694238406613, 8.947790433994205372 ) ) ;
#95115=CARTESIAN_POINT ( 'NONE',  ( -18.01732314745861530, 13.19606014829601826, 11.49999999999998934 ) ) ;
#95117=B_SPLINE_CURVE_WITH_KNOTS ( 'NONE', 3,
 ( #87968, #73246, #65159, #96080 ),
 .UNSPECIFIED., .F., .F.,
 ( 4, 4 ),
 ( 0.2899930013815662511, 0.2989994326536817293 ),
 .UNSPECIFIED. ) ;
#95121=CARTESIAN_POINT ( 'NONE',  ( -42.62287095715004881, -23.47593901973091235, -1.443836447539011525 ) ) ;
#95123=CARTESIAN_POINT ( 'NONE',  ( 20.57277012135545036, 3.371850554975475145, 11.49999999999998934 ) ) ;
#95124=ORIENTED_EDGE ( 'NONE', *, *, #62565, .F. ) ;
#95125=CARTESIAN_POINT ( 'NONE',  ( -79.52287095715009002, -24.51387760970724372, 9.387446482453409402 ) ) ;
#95127=ORIENTED_EDGE ( 'NONE', *, *, #16553, .F. ) ;
#95128=EDGE_CURVE ( 'NONE', #10120, #17101, #95806, .T. ) ;
#95129=CARTESIAN_POINT ( 'NONE',  ( -33.55620429048339304, -23.47593901973091235, -1.443836447539013301 ) ) ;
#95130=CARTESIAN_POINT ( 'NONE',  ( -5.931750313267273533, -20.21149935180699231, -1.500000000000002220 ) ) ;
#95131=EDGE_LOOP ( 'NONE', ( #47834, #21068, #21653, #36648 ) ) ;
#95133=CARTESIAN_POINT ( 'NONE',  ( -93.62287095715005592, -23.48786465467241769, 11.44779295918254114 ) ) ;
#95135=EDGE_CURVE ( 'NONE', #28096, #51004, #72822, .T. ) ;
#95136=CARTESIAN_POINT ( 'NONE',  ( -120.5880710595450722, -24.92592662359561118, 8.075495903017998245 ) ) ;
#95137=VECTOR ( 'NONE', #27632, 1000.000000000000114 ) ;
#95139=CARTESIAN_POINT ( 'NONE',  ( -110.3139465455115271, -25.12049752546738191, 2.832404795212222659 ) ) ;
#95140=CARTESIAN_POINT ( 'NONE',  ( -5.395268184683536639, 21.00466093859614958, -1.500000000000002220 ) ) ;
#95141=CARTESIAN_POINT ( 'NONE',  ( -57.52287095715004739, -23.96127896941631974, -0.6493128931038052443 ) ) ;
#95142=CARTESIAN_POINT ( 'NONE',  ( 7.688942331755139747, 20.87172568467934752, 11.49999999999999645 ) ) ;
#95144=CARTESIAN_POINT ( 'NONE',  ( -51.34258402508250185, -25.24728821302171156, 5.647563055808960009 ) ) ;
#95145=CARTESIAN_POINT ( 'NONE',  ( -70.93618602633573289, -25.29670723202037408, 5.474567338846606290 ) ) ;
#95148=EDGE_CURVE ( 'NONE', #10079, #31190, #50958, .T. ) ;
#95151=ADVANCED_FACE ( 'NONE', ( #18932 ), #78324, .T. ) ;
#95152=ORIENTED_EDGE ( 'NONE', *, *, #44173, .T. ) ;
#95153=ADVANCED_FACE ( 'NONE', ( #65144 ), #35552, .T. ) ;
#95155=CARTESIAN_POINT ( 'NONE',  ( -1.972954090310384379, -20.06304030521763337, 11.49999999999998934 ) ) ;
#95157=ORIENTED_EDGE ( 'NONE', *, *, #26986, .F. ) ;
#95158=CARTESIAN_POINT ( 'NONE',  ( -130.5728709571500588, -24.78459947536195429, 1.143784119390943266 ) ) ;
#95159=CARTESIAN_POINT ( 'NONE',  ( -1.986123035288760885, 22.30159847666916662, -1.500000000000002220 ) ) ;
#95160=VERTEX_POINT ( 'NONE', #56018 ) ;
#95162=CARTESIAN_POINT ( 'NONE',  ( -112.5540285387501171, -24.15620529776628445, 10.23563542870659404 ) ) ;
#95163=CARTESIAN_POINT ( 'NONE',  ( -101.5550256582385344, -23.96169478059713853, 10.65365249895717881 ) ) ;
#95164=CARTESIAN_POINT ( 'NONE',  ( -61.52287095715006160, -24.64965694238407323, 8.947790433994201820 ) ) ;
#95166=CARTESIAN_POINT ( 'NONE',  ( -41.52287095715006870, -24.65952944569304606, 1.056160979905691910 ) ) ;
#95167=CARTESIAN_POINT ( 'NONE',  ( -63.90635886673450017, -25.30559561715417871, 6.147794833475641596 ) ) ;
#95168=CARTESIAN_POINT ( 'NONE',  ( -6.365771329251782795, -18.49506561991874065, -1.500000000000002220 ) ) ;
#95169=B_SPLINE_SURFACE_WITH_KNOTS ( 'NONE', 3, 3, ( 
 ( #84885, #6761, #7256, #46837 ),
 ( #69166, #99103, #45837, #29600 ),
 ( #47337, #68675, #53956, #8772 ),
 ( #99595, #39709, #83887, #91496 ),
 ( #60579, #31097, #46330, #21974 ),
 ( #30098, #52956, #77261, #91999 ),
 ( #154, #53460, #14369, #76756 ) ),
 .UNSPECIFIED., .F., .F., .F.,
 ( 4, 3, 4 ),
 ( 4, 4 ),
 ( 0.7945040050992241421, 0.8970133687736498995, 0.9995227324480755460 ),
 ( 0.2095472461047292734, 0.2106567115738801899 ),
 .UNSPECIFIED. ) ;
#95170=CARTESIAN_POINT ( 'NONE',  ( -50.38822539166535108, -25.31267346029541088, 4.736250531364077254 ) ) ;
#95171=ORIENTED_EDGE ( 'NONE', *, *, #45430, .F. ) ;
#95172=CARTESIAN_POINT ( 'NONE',  ( -17.55493245422511350, -12.44833567967518029, -1.500000000000002220 ) ) ;
#95174=CARTESIAN_POINT ( 'NONE',  ( -129.5895376238167387, -24.64965694238408034, 8.947790433994645909 ) ) ;
#95177=LINE ( 'NONE', #89067, #29337 ) ;
#95178=CARTESIAN_POINT ( 'NONE',  ( 5.768980952343642166, -22.17701263744951490, -1.500000000000002220 ) ) ;
#95181=CARTESIAN_POINT ( 'NONE',  ( -53.56762332262419335, -23.48783264082476663, -1.443836473390096353 ) ) ;
#95182=CARTESIAN_POINT ( 'NONE',  ( -14.83682921977595548, 13.52632505182701017, 11.49999999999999645 ) ) ;
#95183=CARTESIAN_POINT ( 'NONE',  ( -127.6228709571500559, -29.50250243563736774, 8.947779886222132717 ) ) ;
#95184=CARTESIAN_POINT ( 'NONE',  ( -32.62928502708932399, -24.51419770103159834, 9.386484678747182286 ) ) ;
#95186=CARTESIAN_POINT ( 'NONE',  ( -121.6228709571499991, -23.95044443724992078, 10.65354141964649237 ) ) ;
#95188=CARTESIAN_POINT ( 'NONE',  ( -50.62287095715005592, -23.48786465467241058, 11.44779295918255180 ) ) ;
#95189=CARTESIAN_POINT ( 'NONE',  ( 19.75055111929153639, -1.948201398878238066, 11.49999999999998934 ) ) ;
#95190=CARTESIAN_POINT ( 'NONE',  ( -94.52287095715004739, -24.50321055353806088, 9.387540953477534700 ) ) ;
#95191=CARTESIAN_POINT ( 'NONE',  ( 19.40334540789412188, 3.064012487144803565, -1.500000000000002220 ) ) ;
#95193=CARTESIAN_POINT ( 'NONE',  ( -75.62287095715005592, -23.48786465467241058, 11.44779295918254647 ) ) ;
#95198=CARTESIAN_POINT ( 'NONE',  ( -11.86786554430972096, -16.85652113839894639, 11.49999999999999645 ) ) ;
#95200=ADVANCED_FACE ( 'NONE', ( #87450 ), #17943, .F. ) ;
#95202=CARTESIAN_POINT ( 'NONE',  ( 22.41689761077644860, -2.907977976681301424, 11.49999999999999645 ) ) ;
#95204=EDGE_CURVE ( 'NONE', #85400, #70110, #80337, .T. ) ;
#95205=CARTESIAN_POINT ( 'NONE',  ( -69.34384048089543739, -25.25639414125907578, 6.239613344031938347 ) ) ;
#95206=FACE_OUTER_BOUND ( 'NONE', #43584, .T. ) ;
#95207=CARTESIAN_POINT ( 'NONE',  ( -109.6228709571500559, -24.50321055353806443, 9.387540953477524042 ) ) ;
#95210=CARTESIAN_POINT ( 'NONE',  ( -110.6228709571500559, -24.99156045073393173, 7.747789690856161648 ) ) ;
#95212=B_SPLINE_CURVE_WITH_KNOTS ( 'NONE', 3,
 ( #74136, #36069, #20324, #4629 ),
 .UNSPECIFIED., .F., .F.,
 ( 4, 4 ),
 ( 0.000000000000000000, 9.999999999998897304E-05 ),
 .UNSPECIFIED. ) ;
#95213=VERTEX_POINT ( 'NONE', #5706 ) ;
#95214=CARTESIAN_POINT ( 'NONE',  ( -80.39192082756260049, -25.26749876446105958, 4.967919919415041186 ) ) ;
#95215=CARTESIAN_POINT ( 'NONE',  ( -21.19308438721250099, -8.479022899233653376, 11.49999999999998934 ) ) ;
#95216=CARTESIAN_POINT ( 'NONE',  ( -98.52287095715006160, -24.64965694238575011, 8.947790433994194714 ) ) ;
#95217=DIRECTION ( 'NONE',  ( 0.000000000000000000, 0.9999999999976377785, 2.173523156925979975E-06 ) ) ;
#95218=CARTESIAN_POINT ( 'NONE',  ( -82.64080038552411622, -23.73791477778911840, 11.05961554403170766 ) ) ;
#95219=CARTESIAN_POINT ( 'NONE',  ( 11.54466316424315231, -19.26756404802103972, 11.49999999999999645 ) ) ;
#95221=DIRECTION ( 'NONE',  ( -3.773278334453080206E-23, 0.9999999999976377785, 2.173523156925979975E-06 ) ) ;
#95222=CARTESIAN_POINT ( 'NONE',  ( 16.22650188657148362, -14.79325693486936188, -1.500000000000002220 ) ) ;
#95223=CARTESIAN_POINT ( 'NONE',  ( -124.4728709570020015, -25.40556190190858388, 4.804048521347549006 ) ) ;
#95224=CARTESIAN_POINT ( 'NONE',  ( -34.50428818987079893, -23.96169478059712077, 10.65365249895718769 ) ) ;
#95225=CARTESIAN_POINT ( 'NONE',  ( -66.62287095715005592, -29.50248528299804818, 1.056150453629036701 ) ) ;
#95226=EDGE_LOOP ( 'NONE', ( #28452, #45716, #55572, #93587 ) ) ;
#95227=DIRECTION ( 'NONE',  ( -3.773278334453079030E-23, 0.9999999999976377785, 2.173523156925979128E-06 ) ) ;
#95228=CARTESIAN_POINT ( 'NONE',  ( -36.62287095715005592, -29.50248528299804818, 1.056150453629031594 ) ) ;
#95230=CARTESIAN_POINT ( 'NONE',  ( -17.09319154528168383, -11.34935287704045948, -1.500000000000002220 ) ) ;
#95231=ORIENTED_EDGE ( 'NONE', *, *, #61451, .F. ) ;
#95236=CARTESIAN_POINT ( 'NONE',  ( 1.767912858038628965, -23.04938964843747584, 11.49999999999998934 ) ) ;
#95238=CARTESIAN_POINT ( 'NONE',  ( -18.18203184671642703, 9.085611141607108365, -1.500000000000002220 ) ) ;
#95240=DIRECTION ( 'NONE',  ( 1.000000000000000000, 3.773278334444167608E-23, 8.201307833595939069E-29 ) ) ;
#95241=CARTESIAN_POINT ( 'NONE',  ( -29.62953203690532433, -24.43865590823392253, 9.386484716961753350 ) ) ;
#95242=CARTESIAN_POINT ( 'NONE',  ( -114.6228709571500417, -23.48786465467241769, 11.44779295918253936 ) ) ;
#95244=CARTESIAN_POINT ( 'NONE',  ( 2.436486579176012413, 21.40072447632485364, 11.49999999999999645 ) ) ;
#95245=ORIENTED_EDGE ( 'NONE', *, *, #25325, .F. ) ;
#95246=CARTESIAN_POINT ( 'NONE',  ( -29.24616400714660003, -24.76881415122372232, 4.855717898223424811 ) ) ;
#95248=ORIENTED_EDGE ( 'NONE', *, *, #34767, .T. ) ;
#95249=CARTESIAN_POINT ( 'NONE',  ( -15.76495264167062160, -13.51897010167481739, 11.49999999999998934 ) ) ;
#95250=ORIENTED_EDGE ( 'NONE', *, *, #92847, .T. ) ;
#95251=DIRECTION ( 'NONE',  ( -3.773278334453080206E-23, 0.9999999999976377785, 2.173523156925979975E-06 ) ) ;
#95253=B_SPLINE_SURFACE_WITH_KNOTS ( 'NONE', 3, 3, ( 
 ( #21083, #6862, #68272, #100179 ),
 ( #83480, #44944, #84484, #60671 ),
 ( #14966, #45937, #99201, #29207 ),
 ( #92094, #29701, #36324, #28712 ),
 ( #59673, #61173, #91594, #7351 ),
 ( #75866, #37814, #68769, #90602 ),
 ( #52049, #82979, #30697, #53055 ),
 ( #6368, #99686, #37328, #23064 ),
 ( #83984, #13470, #14463, #61669 ),
 ( #84979, #44441, #45445, #5865 ) ),
 .UNSPECIFIED., .F., .F., .F.,
 ( 4, 3, 3, 4 ),
 ( 4, 4 ),
 ( 0.7022005934544808259, 0.7765311282028795059, 0.8508616629512781859, 0.9995227324480756570 ),
 ( 0.2495241106790039021, 0.2506855486834824731 ),
 .UNSPECIFIED. ) ;
#95254=CARTESIAN_POINT ( 'NONE',  ( -110.9909297185884327, -29.50249817218807635, 6.986241424688308221 ) ) ;
#95255=PLANE ( 'NONE',  #48702 ) ;
#95258=DIRECTION ( 'NONE',  ( -3.773278334453079618E-23, 0.9999999999976377785, 2.173523156925979975E-06 ) ) ;
#95261=DIRECTION ( 'NONE',  ( -3.773278334453079618E-23, 0.9999999999976377785, 2.173523156925979975E-06 ) ) ;
#95262=CARTESIAN_POINT ( 'NONE',  ( 9.413913215453616701, -19.89622248225912315, 11.49999999999999645 ) ) ;
#95264=CARTESIAN_POINT ( 'NONE',  ( -103.5098641677505213, -24.65952944569305316, 1.056160979905703234 ) ) ;
#95265=EDGE_CURVE ( 'NONE', #84023, #14758, #70282, .T. ) ;
#95266=CARTESIAN_POINT ( 'NONE',  ( 14.59886444729927923, 17.24780449347180067, 11.49999999999998934 ) ) ;
#95269=CARTESIAN_POINT ( 'NONE',  ( -62.52287095715006160, -23.47593901973090169, -1.443836447538997092 ) ) ;
#95270=ORIENTED_EDGE ( 'NONE', *, *, #95022, .T. ) ;
#95271=EDGE_CURVE ( 'NONE', #47459, #20866, #100029, .T. ) ;
#95273=ADVANCED_FACE ( 'NONE', ( #31539 ), #8214, .T. ) ;
#95274=CARTESIAN_POINT ( 'NONE',  ( -83.52287095715001897, -24.66019654487199375, 8.947790411086122830 ) ) ;
#95275=VECTOR ( 'NONE', #89999, 1000.000000000000114 ) ;
#95276=CARTESIAN_POINT ( 'NONE',  ( -86.62287095715004170, -23.48783264082478794, -1.443836473390063713 ) ) ;
#95278=CARTESIAN_POINT ( 'NONE',  ( -16.93204426113827310, 12.72334981527875186, -1.500000000000002220 ) ) ;
#95279=CARTESIAN_POINT ( 'NONE',  ( -82.62287095715008434, -24.51283580621365132, 0.6167428607019763698 ) ) ;
#95281=VECTOR ( 'NONE', #90909, 1000.000000000000114 ) ;
#95283=CARTESIAN_POINT ( 'NONE',  ( -40.84407949893366663, -25.29514021929367118, 5.506588697105319952 ) ) ;
#95284=CARTESIAN_POINT ( 'NONE',  ( -21.61287440533560300, 5.199345243644041936, -1.500000000000002220 ) ) ;
#95285=CARTESIAN_POINT ( 'NONE',  ( -67.62287095715005592, -29.50250243563736774, 8.947779886222143375 ) ) ;
#95286=EDGE_CURVE ( 'NONE', #46066, #65965, #61854, .T. ) ;
#95290=CARTESIAN_POINT ( 'NONE',  ( -15.38109395195050233, 11.78095549196778258, 11.49999999999999645 ) ) ;
#95291=CARTESIAN_POINT ( 'NONE',  ( -36.65742501572457712, -23.73791477778911130, 11.05961554403171121 ) ) ;
#95293=CARTESIAN_POINT ( 'NONE',  ( 19.19537281719634336, 3.394423509666608663, -1.500000000000002220 ) ) ;
#95294=CARTESIAN_POINT ( 'NONE',  ( 14.52366289275476419, -15.72616519631134580, -1.500000000000002220 ) ) ;
#95296=CARTESIAN_POINT ( 'NONE',  ( -60.60738981642156631, -23.85049219812968602, 10.88485053497088728 ) ) ;
#95298=CARTESIAN_POINT ( 'NONE',  ( -77.62361607832929167, -24.65952944569304606, 1.056160979905701458 ) ) ;
#95299=CARTESIAN_POINT ( 'NONE',  ( 21.15473741701296362, -8.388382055385795510, -1.500000000000002220 ) ) ;
#95301=CARTESIAN_POINT ( 'NONE',  ( -98.51385245561148452, -24.15543982623907482, -0.2315651400026625395 ) ) ;
#95303=CARTESIAN_POINT ( 'NONE',  ( -19.80664267627650688, 2.137978742899185214, 11.49999999999999645 ) ) ;
#95304=CARTESIAN_POINT ( 'NONE',  ( -123.5911770222576251, -23.73791477778912551, 11.05961554403169878 ) ) ;
#95306=DIRECTION ( 'NONE',  ( -0.8209519386396718632, 0.000000000000000000, -0.5709972981054852736 ) ) ;
#95309=CARTESIAN_POINT ( 'NONE',  ( -31.23323026593057250, -24.87479601683088148, 8.247789944647561100 ) ) ;
#95310=CARTESIAN_POINT ( 'NONE',  ( -63.58953762381672448, -23.48786465467241058, 11.44779295918254824 ) ) ;
#95311=CARTESIAN_POINT ( 'NONE',  ( -12.04083774165243881, -18.01462592983040523, 11.49999999999998934 ) ) ;
#95312=CARTESIAN_POINT ( 'NONE',  ( -51.91099744296860763, -25.23365410514359652, 6.412898804246325746 ) ) ;
#95313=CARTESIAN_POINT ( 'NONE',  ( -0.2416374764669896869, -19.45557994585427508, -1.500000000000002220 ) ) ;
#95314=CARTESIAN_POINT ( 'NONE',  ( -58.62287095715004881, -29.50248528299804818, 1.056150453629034924 ) ) ;
#95315=B_SPLINE_CURVE_WITH_KNOTS ( 'NONE', 3,
 ( #38280, #44921, #68248, #99663 ),
 .UNSPECIFIED., .F., .F.,
 ( 4, 4 ),
 ( 0.04878993775236183800, 0.04979068479312719064 ),
 .UNSPECIFIED. ) ;
#95316=EDGE_CURVE ( 'NONE', #93197, #28046, #21912, .T. ) ;
#95317=ORIENTED_EDGE ( 'NONE', *, *, #42191, .T. ) ;
#95318=CARTESIAN_POINT ( 'NONE',  ( -102.6228709571500559, -29.50250243563736774, 8.947779886222138046 ) ) ;
#95319=CARTESIAN_POINT ( 'NONE',  ( 11.27307661227339430, 16.98952936956587934, 11.49999999999999645 ) ) ;
#95320=PLANE ( 'NONE',  #6724 ) ;
#95321=ADVANCED_FACE ( 'NONE', ( #46776 ), #97921, .T. ) ;
#95322=CARTESIAN_POINT ( 'NONE',  ( -59.90086478509797985, -25.28839794021433462, 4.072426394371103875 ) ) ;
#95327=CARTESIAN_POINT ( 'NONE',  ( -125.5228709571500616, -23.48786465467241769, 11.44779295918253581 ) ) ;
#95331=CARTESIAN_POINT ( 'NONE',  ( -66.50542857718694734, -24.15620529776628089, 10.23563542870660470 ) ) ;
#95333=CARTESIAN_POINT ( 'NONE',  ( -21.95939045666098366, -6.591442671832903777, 11.49999999999999645 ) ) ;
#95334=CARTESIAN_POINT ( 'NONE',  ( -12.51292883401962541, 18.98408452820241266, -1.500000000000002220 ) ) ;
#95336=CARTESIAN_POINT ( 'NONE',  ( -68.52287095715006160, -24.64965694238407323, 8.947790433994200043 ) ) ;
#95338=CARTESIAN_POINT ( 'NONE',  ( -69.90276568578059369, -25.14717367798247594, 7.019980506270512066 ) ) ;
#95339=CARTESIAN_POINT ( 'NONE',  ( -19.20277006422315225, 10.48866939257135833, 11.49999999999998934 ) ) ;
#95341=CARTESIAN_POINT ( 'NONE',  ( -69.53738162378759569, -24.66019654487199375, 8.947790411086119278 ) ) ;
#95342=CARTESIAN_POINT ( 'NONE',  ( -26.26995961867267937, -24.88333753901390466, 3.525190991172063804 ) ) ;
#95344=CARTESIAN_POINT ( 'NONE',  ( -58.60466252300279422, -23.73766607897669800, -1.055555164236457344 ) ) ;
#95346=B_SPLINE_CURVE_WITH_KNOTS ( 'NONE', 3,
 ( #50787, #81228, #65533, #26452 ),
 .UNSPECIFIED., .F., .F.,
 ( 4, 4 ),
 ( 0.5992008101734043191, 0.6002015572141699007 ),
 .UNSPECIFIED. ) ;
#95348=CARTESIAN_POINT ( 'NONE',  ( -20.22731604866883970, -2.807383831903240257, 11.49999999999998934 ) ) ;
#95349=VERTEX_POINT ( 'NONE', #78696 ) ;
#95351=CARTESIAN_POINT ( 'NONE',  ( 8.869223403490039459, -21.23658630136709391, 11.49999999999998934 ) ) ;
#95352=CARTESIAN_POINT ( 'NONE',  ( -80.52287095714999055, -24.92579138211018730, 1.929029949965667567 ) ) ;
#95353=ORIENTED_EDGE ( 'NONE', *, *, #31388, .T. ) ;
#95354=DIRECTION ( 'NONE',  ( -3.773278334453079030E-23, 0.9999999999976377785, 2.173523156925979128E-06 ) ) ;
#95355=CARTESIAN_POINT ( 'NONE',  ( -78.52287095715006160, -23.47596703998600631, 11.44779298504228571 ) ) ;
#95357=CARTESIAN_POINT ( 'NONE',  ( -118.1692254313890231, -25.21288489780929964, 6.500946880900415614 ) ) ;
#95358=VECTOR ( 'NONE', #44918, 1000.000000000000114 ) ;
#95359=CARTESIAN_POINT ( 'NONE',  ( -11.21157863559261791, -18.18922556752850994, 11.49999999999999645 ) ) ;
#95360=ORIENTED_EDGE ( 'NONE', *, *, #31016, .F. ) ;
#95361=ORIENTED_EDGE ( 'NONE', *, *, #41552, .F. ) ;
#95362=CARTESIAN_POINT ( 'NONE',  ( -8.951960448472247478, 20.35530821588910300, -1.500000000000002220 ) ) ;
#95363=CARTESIAN_POINT ( 'NONE',  ( 18.09409571311175569, -9.955296453752364272, -1.500000000000002220 ) ) ;
#95367=EDGE_LOOP ( 'NONE', ( #100225, #29244, #686, #83865 ) ) ;
#95368=CARTESIAN_POINT ( 'NONE',  ( -111.6228709571500559, -23.47593901973091235, -1.443836447538999312 ) ) ;
#95369=B_SPLINE_CURVE_WITH_KNOTS ( 'NONE', 3,
 ( #37051, #67026, #91832, #83219 ),
 .UNSPECIFIED., .F., .F.,
 ( 4, 4 ),
 ( 0.000000000000000000, 9.999999999999591193E-05 ),
 .UNSPECIFIED. ) ;
#95373=CARTESIAN_POINT ( 'NONE',  ( 16.15719879640481338, -13.26386290209467944, -1.500000000000002220 ) ) ;
#95375=CARTESIAN_POINT ( 'NONE',  ( 9.643594380127815668, 19.59848315111488759, 11.49999999999999645 ) ) ;
#95376=CARTESIAN_POINT ( 'NONE',  ( -73.59227796171214209, -24.15620529776628089, 10.23563542870660470 ) ) ;
#95377=CARTESIAN_POINT ( 'NONE',  ( -37.62287095715007013, -24.34917612406837861, 0.1852690917426592920 ) ) ;
#95378=CARTESIAN_POINT ( 'NONE',  ( 20.54305097139451064, 9.177977666691313985, 11.49999999999998934 ) ) ;
#95379=CARTESIAN_POINT ( 'NONE',  ( 12.70736309587848645, -16.60074808024427284, 11.49999999999998934 ) ) ;
#95380=CARTESIAN_POINT ( 'NONE',  ( -38.53316654600265423, -24.51314013834316086, 0.6176544820404135105 ) ) ;
#95385=ORIENTED_EDGE ( 'NONE', *, *, #23117, .T. ) ;
#95386=ORIENTED_EDGE ( 'NONE', *, *, #92933, .F. ) ;
#95388=CARTESIAN_POINT ( 'NONE',  ( -99.29755759592676156, -25.26221118157064538, 6.181036435632247361 ) ) ;
#95389=ORIENTED_EDGE ( 'NONE', *, *, #23812, .F. ) ;
#95390=CARTESIAN_POINT ( 'NONE',  ( -11.99125074976391048, 17.70416384622758343, -1.500000000000002220 ) ) ;
#95391=CARTESIAN_POINT ( 'NONE',  ( -20.95026660567425481, -7.857139728745305973, 11.49999999999999645 ) ) ;
#95392=VERTEX_POINT ( 'NONE', #47783 ) ;
#95393=CARTESIAN_POINT ( 'NONE',  ( -26.29209366616924015, -24.89473993083786851, 6.397464118119456700 ) ) ;
#95394=CARTESIAN_POINT ( 'NONE',  ( 5.245434476726341444, -20.39595507048906242, 11.49999999999998934 ) ) ;
#95395=CARTESIAN_POINT ( 'NONE',  ( -30.60461477208441750, -24.58290936297911955, 9.174392229302920754 ) ) ;
#95396=CARTESIAN_POINT ( 'NONE',  ( 19.92730240972663935, 0.8534881809820089593, -1.500000000000002220 ) ) ;
#95398=CARTESIAN_POINT ( 'NONE',  ( -50.47484537770900204, -25.00182538069147142, 7.747789668545043362 ) ) ;
#95399=CARTESIAN_POINT ( 'NONE',  ( -101.6251937039718598, -24.51314013834316086, 0.6176544820404198388 ) ) ;
#95400=CARTESIAN_POINT ( 'NONE',  ( 19.60348439636399931, 10.09110264789753053, -1.500000000000002220 ) ) ;
#95402=CARTESIAN_POINT ( 'NONE',  ( -65.61529913176147488, -23.48786465467241058, 11.44779295918254824 ) ) ;
#95403=EDGE_CURVE ( 'NONE', #52326, #94778, #86335, .T. ) ;
#95404=B_SPLINE_CURVE_WITH_KNOTS ( 'NONE', 3,
 ( #5203, #75699, #13301, #82818 ),
 .UNSPECIFIED., .F., .F.,
 ( 4, 4 ),
 ( 0.000000000000000000, 9.999999999998897304E-05 ),
 .UNSPECIFIED. ) ;
#95405=CARTESIAN_POINT ( 'NONE',  ( -109.6228709571500559, -29.50250243563736774, 8.947779886222136270 ) ) ;
#95406=CARTESIAN_POINT ( 'NONE',  ( -60.57813654160024441, -24.92564183028978420, 1.928384488918252648 ) ) ;
#95407=VECTOR ( 'NONE', #91735, 1000.000000000000114 ) ;
#95408=CARTESIAN_POINT ( 'NONE',  ( -62.50953048082695318, -23.96169478059712787, 10.65365249895718414 ) ) ;
#95410=DIRECTION ( 'NONE',  ( -3.773278334453080206E-23, 0.9999999999976377785, 2.173523156925979975E-06 ) ) ;
#95411=CARTESIAN_POINT ( 'NONE',  ( 3.065528897535349628, -21.08962430476942274, -1.500000000000002220 ) ) ;
#95412=CARTESIAN_POINT ( 'NONE',  ( -104.5228709571500758, -23.73934037231757443, 11.05740245334328087 ) ) ;
#95413=CARTESIAN_POINT ( 'NONE',  ( -124.5228709571500332, -23.94994826722565762, -0.6494450866342719175 ) ) ;
#95414=FACE_OUTER_BOUND ( 'NONE', #36580, .T. ) ;
#95415=CARTESIAN_POINT ( 'NONE',  ( -114.6228709571500559, -24.64898659630528854, 1.056161002820831474 ) ) ;
#95416=CARTESIAN_POINT ( 'NONE',  ( 5.419076944403256491, 21.93356404788375258, -1.500000000000002220 ) ) ;
#95417=DIRECTION ( 'NONE',  ( 0.000000000000000000, -2.173523156925980399E-06, 0.9999999999976378895 ) ) ;
#95418=ORIENTED_EDGE ( 'NONE', *, *, #51494, .T. ) ;
#95420=CARTESIAN_POINT ( 'NONE',  ( -31.62934438217061839, -24.51419770103156637, 9.386484678747187615 ) ) ;
#95421=CARTESIAN_POINT ( 'NONE',  ( -18.74838588596843181, -5.942601993926947657, 11.49999999999999645 ) ) ;
#95422=DIRECTION ( 'NONE',  ( 0.000000000000000000, 2.173523156925980399E-06, -0.9999999999976378895 ) ) ;
#95424=FACE_OUTER_BOUND ( 'NONE', #37531, .T. ) ;
#95427=CARTESIAN_POINT ( 'NONE',  ( -42.62287095715004881, -23.47593901973091235, -1.443836447539011525 ) ) ;
#95428=CARTESIAN_POINT ( 'NONE',  ( -39.62287095715005592, -24.65952944569304606, 1.056160979905692354 ) ) ;
#95429=CARTESIAN_POINT ( 'NONE',  ( -122.6228709571500417, -24.64898659630368627, 1.056161002820833028 ) ) ;
#95430=PLANE ( 'NONE',  #72892 ) ;
#95431=CARTESIAN_POINT ( 'NONE',  ( -76.52287095715007581, -24.66019654487199730, 8.947790411086124607 ) ) ;
#95433=CARTESIAN_POINT ( 'NONE',  ( -16.86558833231006460, 10.32443627698238409, 11.49999999999998934 ) ) ;
#95435=CARTESIAN_POINT ( 'NONE',  ( -0.9278407348523283193, 20.21260682001012654, 11.49999999999999645 ) ) ;
#95438=ADVANCED_FACE ( 'NONE', ( #54895 ), #8717, .F. ) ;
#95439=ORIENTED_EDGE ( 'NONE', *, *, #44620, .T. ) ;
#95441=CARTESIAN_POINT ( 'NONE',  ( -72.62287095715005592, -23.47596703998600631, 11.44779298504227860 ) ) ;
#95443=FACE_OUTER_BOUND ( 'NONE', #45571, .T. ) ;
#95444=CARTESIAN_POINT ( 'NONE',  ( -39.62287095715005592, -23.96127896941631619, -0.6493128931037891460 ) ) ;
#95445=DIRECTION ( 'NONE',  ( -3.773278334453079030E-23, 0.9999999999976377785, 2.173523156925979128E-06 ) ) ;
#95446=CARTESIAN_POINT ( 'NONE',  ( 20.03642891561555928, 0.6179553080306146029, -1.500000000000002220 ) ) ;
#95448=ORIENTED_EDGE ( 'NONE', *, *, #11217, .T. ) ;
#95449=CARTESIAN_POINT ( 'NONE',  ( -58.52287095715009713, -24.66019654487199730, 8.947790411086121054 ) ) ;
#95450=PLANE ( 'NONE',  #70438 ) ;
#95453=CARTESIAN_POINT ( 'NONE',  ( -101.4436883411118515, -25.18151332244121221, 3.266733668633749588 ) ) ;
#95454=ADVANCED_FACE ( 'NONE', ( #19189 ), #40164, .F. ) ;
#95456=CARTESIAN_POINT ( 'NONE',  ( -98.87392103467360016, -25.32724633150700200, 4.398074151685131383 ) ) ;
#95457=ORIENTED_EDGE ( 'NONE', *, *, #3414, .T. ) ;
#95458=ADVANCED_FACE ( 'NONE', ( #2117 ), #54277, .T. ) ;
#95459=AXIS2_PLACEMENT_3D ( 'NONE', #44933, #68261, #236 ) ;
#95460=CARTESIAN_POINT ( 'NONE',  ( -5.305567426876419468, 19.62801697144059787, 11.49999999999998934 ) ) ;
#95463=CARTESIAN_POINT ( 'NONE',  ( -127.5552447816560857, -24.51419770103158768, 9.386484678747160970 ) ) ;
#95465=ORIENTED_EDGE ( 'NONE', *, *, #25894, .T. ) ;
#95467=CARTESIAN_POINT ( 'NONE',  ( -88.55620429048337883, -23.48786465467241058, 11.44779295918254647 ) ) ;
#95469=CARTESIAN_POINT ( 'NONE',  ( -49.94169464672810221, -25.26264163214096570, 7.031227749355628553 ) ) ;
#95470=AXIS2_PLACEMENT_3D ( 'NONE', #28948, #8618, #96236 ) ;
#95471=CARTESIAN_POINT ( 'NONE',  ( -30.47287095715007155, -25.11030793521390692, 2.751272914309959017 ) ) ;
#95472=CARTESIAN_POINT ( 'NONE',  ( -8.144517828999388698, 19.50133175306300970, 11.49999999999999645 ) ) ;
#95473=EDGE_CURVE ( 'NONE', #62593, #48556, #83582, .T. ) ;
#95475=CARTESIAN_POINT ( 'NONE',  ( 8.970247382295582383, 20.24485829007567617, 11.49999999999998934 ) ) ;
#95476=CARTESIAN_POINT ( 'NONE',  ( -16.28974412851428255, -12.55652860423730388, 11.49999999999998934 ) ) ;
#95477=EDGE_LOOP ( 'NONE', ( #58321, #7834, #50940, #54706 ) ) ;
#95478=CARTESIAN_POINT ( 'NONE',  ( -41.63441546978912555, -24.34968618360933590, 0.1864209137778856940 ) ) ;
#95479=ORIENTED_EDGE ( 'NONE', *, *, #57807, .F. ) ;
#95480=DIRECTION ( 'NONE',  ( -0.000000000000000000, 2.173523156925979552E-06, -0.9999999999976378895 ) ) ;
#95481=CARTESIAN_POINT ( 'NONE',  ( -109.5228709571500758, -23.72773821059536914, 11.05748984161097503 ) ) ;
#95482=VERTEX_POINT ( 'NONE', #36418 ) ;
#95483=VERTEX_POINT ( 'NONE', #45541 ) ;
#95485=ORIENTED_EDGE ( 'NONE', *, *, #21808, .F. ) ;
#95486=CARTESIAN_POINT ( 'NONE',  ( -100.5228709571500758, -23.47593901973090524, -1.443836447538996648 ) ) ;
#95489=CARTESIAN_POINT ( 'NONE',  ( -17.26476610439243231, 11.37957233835482818, -1.500000000000002220 ) ) ;
#95491=CARTESIAN_POINT ( 'NONE',  ( 11.52859134480388903, -18.33581920571378632, 11.49999999999999645 ) ) ;
#95493=CARTESIAN_POINT ( 'NONE',  ( -60.52287095715003318, -24.83620972995333531, 8.398175272756253307 ) ) ;
#95495=CARTESIAN_POINT ( 'NONE',  ( 6.968497804723354783, -21.30229754059623559, -1.500000000000002220 ) ) ;
#95496=DIRECTION ( 'NONE',  ( -3.773278334453079030E-23, 0.9999999999976377785, 2.173523156925979128E-06 ) ) ;
#95498=ORIENTED_EDGE ( 'NONE', *, *, #10044, .F. ) ;
#95499=B_SPLINE_CURVE_WITH_KNOTS ( 'NONE', 3,
 ( #13919, #50502, #82931, #83430, #60625, #21524, #12429, #75321 ),
 .UNSPECIFIED., .F., .F.,
 ( 4, 2, 2, 4 ),
 ( -0.001240666984356067221, -0.0002401179793396696679, 0.0007604310256767278856, 0.002761529035709522992 ),
 .UNSPECIFIED. ) ;
#95501=VERTEX_POINT ( 'NONE', #12580 ) ;
#95505=VERTEX_POINT ( 'NONE', #91691 ) ;
#95506=DIRECTION ( 'NONE',  ( -3.773278334453080206E-23, 0.9999999999976377785, 2.173523156925979975E-06 ) ) ;
#95507=CARTESIAN_POINT ( 'NONE',  ( 1.567330217057175901, -21.20382687294985047, -1.500000000000002220 ) ) ;
#95509=ORIENTED_EDGE ( 'NONE', *, *, #55903, .T. ) ;
#95510=CARTESIAN_POINT ( 'NONE',  ( -101.1410787236130489, -25.15676149906418857, 6.899366854011507399 ) ) ;
#95511=CARTESIAN_POINT ( 'NONE',  ( 12.66963027563507005, -17.75133666976559255, 11.49999999999998934 ) ) ;
#95512=CARTESIAN_POINT ( 'NONE',  ( -103.5195636159563719, -23.73791477778911840, 11.05961554403170410 ) ) ;
#95513=CARTESIAN_POINT ( 'NONE',  ( -62.52287095715003318, -24.66019654487199730, 8.947790411086124607 ) ) ;
#95515=CARTESIAN_POINT ( 'NONE',  ( 21.14253370195585546, 5.708146584608840612, -1.500000000000002220 ) ) ;
#95519=FACE_OUTER_BOUND ( 'NONE', #70771, .T. ) ;
#95520=EDGE_CURVE ( 'NONE', #59433, #45083, #98810, .T. ) ;
#95522=ORIENTED_EDGE ( 'NONE', *, *, #25606, .T. ) ;
#95523=CARTESIAN_POINT ( 'NONE',  ( -99.62287095715007013, -24.50321055353805022, 9.387540953477524042 ) ) ;
#95524=EDGE_CURVE ( 'NONE', #52082, #99074, #41173, .T. ) ;
#95527=CARTESIAN_POINT ( 'NONE',  ( -82.62937087436195327, -24.34968618360933945, 0.1864209137778926328 ) ) ;
#95528=CARTESIAN_POINT ( 'NONE',  ( 21.23515499356076930, 0.7789969333488580006, -1.500000000000002220 ) ) ;
#95529=DIRECTION ( 'NONE',  ( -3.773278334453080206E-23, 0.9999999999976377785, 2.173523156925979552E-06 ) ) ;
#95530=CARTESIAN_POINT ( 'NONE',  ( -130.5728709571500588, -24.92410949913934104, 1.600845668900850116 ) ) ;
#95532=CARTESIAN_POINT ( 'NONE',  ( -109.5228709571500616, -23.47596703998600631, 11.44779298504228038 ) ) ;
#95533=CARTESIAN_POINT ( 'NONE',  ( -13.55963120218723361, -13.89248740512243430, -1.500000000000002220 ) ) ;
#95534=CARTESIAN_POINT ( 'NONE',  ( -80.55620429048339304, -23.48786465467240703, 11.44779295918254824 ) ) ;
#95536=CARTESIAN_POINT ( 'NONE',  ( -19.51626497420292239, -0.3564122556526727048, 11.49999999999999645 ) ) ;
#95539=B_SPLINE_CURVE_WITH_KNOTS ( 'NONE', 3,
 ( #11755, #97979, #34111, #81275 ),
 .UNSPECIFIED., .F., .F.,
 ( 4, 4 ),
 ( 0.000000000000000000, 9.999999999998897304E-05 ),
 .UNSPECIFIED. ) ;
#95540=CARTESIAN_POINT ( 'NONE',  ( -80.19178569327479522, -25.12886892462663369, 7.067847742069440109 ) ) ;
#95543=PLANE ( 'NONE',  #96606 ) ;
#95545=DIRECTION ( 'NONE',  ( 3.773278334444167608E-23, -1.000000000000000000, 0.000000000000000000 ) ) ;
#95546=CARTESIAN_POINT ( 'NONE',  ( -81.67724764284677974, -25.03155920135590762, 6.915644353864915495 ) ) ;
#95547=CARTESIAN_POINT ( 'NONE',  ( -3.718233408413001762, 19.32670252783854536, 11.49999999999998934 ) ) ;
#95552=CARTESIAN_POINT ( 'NONE',  ( -18.41700849636773540, 13.91914711744011157, -1.500000000000002220 ) ) ;
#95555=VERTEX_POINT ( 'NONE', #98301 ) ;
#95556=CARTESIAN_POINT ( 'NONE',  ( -63.62287095715004881, -29.50250243563736774, 8.947779886222145151 ) ) ;
#95558=CARTESIAN_POINT ( 'NONE',  ( -114.5895376238167245, -24.64898659630528854, 1.056161002820831252 ) ) ;
#95559=CARTESIAN_POINT ( 'NONE',  ( -97.59370094711790955, -23.96169478059714208, 10.65365249895717703 ) ) ;
#95560=CARTESIAN_POINT ( 'NONE',  ( -81.90499567650900303, -25.14083923594767356, 2.947789366383930965 ) ) ;
#95562=CARTESIAN_POINT ( 'NONE',  ( -73.52287095715006160, -23.72747288104470087, -1.053458166803226570 ) ) ;
#95563=CARTESIAN_POINT ( 'NONE',  ( -8.676013072486071565, -17.92234406281952275, -1.500000000000002220 ) ) ;
#95564=CARTESIAN_POINT ( 'NONE',  ( -75.49751960664619332, -24.63419186844611275, 9.035850630976923981 ) ) ;
#95565=CARTESIAN_POINT ( 'NONE',  ( -15.96263503330635380, 11.84234753045382682, -1.500000000000002220 ) ) ;
#95566=EDGE_LOOP ( 'NONE', ( #27031, #70645, #18617, #75369 ) ) ;
#95567=LINE ( 'NONE', #72744, #29703 ) ;
#95568=CARTESIAN_POINT ( 'NONE',  ( -51.05935189857146383, -25.15701052765065882, 6.962205197853442940 ) ) ;
#95571=CARTESIAN_POINT ( 'NONE',  ( -19.91680486407696904, 5.911688619927280008, 11.49999999999999645 ) ) ;
#95574=CARTESIAN_POINT ( 'NONE',  ( 7.824713763024562674, 21.46283361357968289, 11.49999999999999645 ) ) ;
#95575=VERTEX_POINT ( 'NONE', #51654 ) ;
#95576=ADVANCED_FACE ( 'NONE', ( #75463 ), #53158, .T. ) ;
#95577=CARTESIAN_POINT ( 'NONE',  ( -108.5562042904834072, -24.64965694238575011, 8.947790433994187609 ) ) ;
#95578=CARTESIAN_POINT ( 'NONE',  ( -127.5222628909410645, -23.48783264082477373, -1.443836473390084363 ) ) ;
#95579=ORIENTED_EDGE ( 'NONE', *, *, #26447, .F. ) ;
#95580=CARTESIAN_POINT ( 'NONE',  ( -16.41926757845921614, -11.79510067912178606, 11.49999999999998934 ) ) ;
#95582=CARTESIAN_POINT ( 'NONE',  ( -110.5228709571500616, -25.00182538069145366, 7.747789668545101094 ) ) ;
#95584=EDGE_CURVE ( 'NONE', #20835, #47459, #76375, .T. ) ;
#95586=EDGE_CURVE ( 'NONE', #73913, #69024, #75119, .T. ) ;
#95587=ORIENTED_EDGE ( 'NONE', *, *, #14394, .F. ) ;
#95588=PLANE ( 'NONE',  #9564 ) ;
#95589=CARTESIAN_POINT ( 'NONE',  ( -100.6228709571500417, -24.62226745350440638, 0.9660975649729649506 ) ) ;
#95590=CARTESIAN_POINT ( 'NONE',  ( 16.76344175524385705, -10.90933549886441156, -1.500000000000002220 ) ) ;
#95591=CARTESIAN_POINT ( 'NONE',  ( 12.86141378215833342, 16.59024694808438127, 11.49999999999999645 ) ) ;
#95592=ADVANCED_FACE ( 'NONE', ( #52646 ), #8084, .T. ) ;
#95595=CARTESIAN_POINT ( 'NONE',  ( 18.22792733936863030, -12.41963300964812156, -1.500000000000002220 ) ) ;
#95597=CARTESIAN_POINT ( 'NONE',  ( -39.93582354980947002, -25.31589308170816821, 4.982375540116844803 ) ) ;
#95599=PLANE ( 'NONE',  #77771 ) ;
#95600=CARTESIAN_POINT ( 'NONE',  ( -118.5228709571500758, -23.48786465467241769, 11.44779295918253759 ) ) ;
#95602=ORIENTED_EDGE ( 'NONE', *, *, #74955, .F. ) ;
#95603=DIRECTION ( 'NONE',  ( 0.000000000000000000, -2.173523156925979552E-06, 0.9999999999976378895 ) ) ;
#95607=DIRECTION ( 'NONE',  ( -1.000000000000000000, -3.773278334444167608E-23, -8.201307833595939069E-29 ) ) ;
#95608=CARTESIAN_POINT ( 'NONE',  ( -72.62287095715004170, -23.48786465467241058, 11.44779295918254647 ) ) ;
#95610=CARTESIAN_POINT ( 'NONE',  ( -7.444040098415714013, -19.11467064512029879, -1.500000000000002220 ) ) ;
#95612=ORIENTED_EDGE ( 'NONE', *, *, #10854, .F. ) ;
#95613=CARTESIAN_POINT ( 'NONE',  ( -66.62287095715005592, -29.50250786944525672, 11.44777988621623699 ) ) ;
#95617=CARTESIAN_POINT ( 'NONE',  ( 11.81759748825469281, -18.92407201980706333, -1.500000000000002220 ) ) ;
#95618=CARTESIAN_POINT ( 'NONE',  ( -102.5228709571500758, -23.47596703998600631, 11.44779298504228215 ) ) ;
#95619=DIRECTION ( 'NONE',  ( -3.773278334453079618E-23, 0.9999999999976377785, 2.173523156925978705E-06 ) ) ;
#95621=EDGE_LOOP ( 'NONE', ( #20273, #82209, #13132, #83425 ) ) ;
#95622=CARTESIAN_POINT ( 'NONE',  ( -104.5228709571500758, -24.66019654487200441, 8.947790411086113949 ) ) ;
#95623=VECTOR ( 'NONE', #73155, 1000.000000000000114 ) ;
#95626=CARTESIAN_POINT ( 'NONE',  ( 19.93353245626563819, -6.116835970281883306, -1.500000000000002220 ) ) ;
#95627=ORIENTED_EDGE ( 'NONE', *, *, #18090, .F. ) ;
#95629=EDGE_CURVE ( 'NONE', #20120, #7838, #53396, .T. ) ;
#95633=CARTESIAN_POINT ( 'NONE',  ( -68.94101663640660149, -25.03149086959048120, 6.247842836060496730 ) ) ;
#95634=CARTESIAN_POINT ( 'NONE',  ( -16.48755246578841849, -13.11705038010048163, -1.500000000000002220 ) ) ;
#95635=ORIENTED_EDGE ( 'NONE', *, *, #88733, .T. ) ;
#95636=DIRECTION ( 'NONE',  ( -3.773278334453079030E-23, 0.9999999999976377785, 2.173523156925978705E-06 ) ) ;
#95638=CARTESIAN_POINT ( 'NONE',  ( -120.5877765925405640, -25.00182538069146787, 7.747789668545044250 ) ) ;
#95639=CARTESIAN_POINT ( 'NONE',  ( -100.8646123533485621, -25.25419544284016737, 7.517421368992579289 ) ) ;
#95640=CARTESIAN_POINT ( 'NONE',  ( -59.62769267835140852, -24.51314013834316441, 0.6176544820404136216 ) ) ;
#95641=CARTESIAN_POINT ( 'NONE',  ( -1.268225406894735396, -21.67698866206750097, -1.500000000000002220 ) ) ;
#95642=CARTESIAN_POINT ( 'NONE',  ( -107.6228709571500701, -23.48783264082479150, -1.443836473390060382 ) ) ;
#95643=CARTESIAN_POINT ( 'NONE',  ( 21.27325221474336914, 6.521069146585026566, 11.49999999999999645 ) ) ;
#95644=VERTEX_POINT ( 'NONE', #351 ) ;
#95645=CARTESIAN_POINT ( 'NONE',  ( -57.52287095715005449, -29.50250786944525672, 11.44777988621623876 ) ) ;
#95647=CARTESIAN_POINT ( 'NONE',  ( -71.30457154551152144, -25.24554880456021522, 6.209207408033732278 ) ) ;
#95648=ADVANCED_FACE ( 'NONE', ( #94192 ), #4755, .T. ) ;
#95649=ORIENTED_EDGE ( 'NONE', *, *, #29372, .F. ) ;
#95650=EDGE_CURVE ( 'NONE', #32345, #98224, #10975, .T. ) ;
#95652=ORIENTED_EDGE ( 'NONE', *, *, #18653, .T. ) ;
#95655=EDGE_CURVE ( 'NONE', #65926, #58835, #21914, .T. ) ;
#95656=B_SPLINE_CURVE_WITH_KNOTS ( 'NONE', 3,
 ( #86161, #56736, #55733, #48114, #25258, #56237 ),
 .UNSPECIFIED., .F., .F.,
 ( 4, 2, 4 ),
 ( 0.000000000000000000, 0.001380901958385385509, 0.002761803916770771018 ),
 .UNSPECIFIED. ) ;
#95657=CARTESIAN_POINT ( 'NONE',  ( -48.62287095715004881, -24.65952944569303895, 1.056160979905692798 ) ) ;
#95658=CARTESIAN_POINT ( 'NONE',  ( -51.52287095715009713, -24.33927499327855060, 9.819080762295804732 ) ) ;
#95659=ORIENTED_EDGE ( 'NONE', *, *, #88194, .F. ) ;
#95660=B_SPLINE_CURVE_WITH_KNOTS ( 'NONE', 3,
 ( #15485, #55573, #14991, #62688, #70789, #53582, #47452, #38329, #1283, #31723, #69287, #16481, #100203, #38828, #30721, #93604, #8885, #39829, #61690, #23089 ),
 .UNSPECIFIED., .F., .F.,
 ( 4, 2, 2, 2, 2, 2, 2, 2, 2, 4 ),
 ( 0.000000000000000000, 0.0005520169820108884132, 0.001104033964021776826, 0.001656050946032664156, 0.002208067928043551485, 0.002760084910054437946, 0.003312101892065325275, 0.003864118874076212171, 0.004140127365081655401, 0.004416135856087097765 ),
 .UNSPECIFIED. ) ;
#95661=CARTESIAN_POINT ( 'NONE',  ( -130.5728709571500588, -25.19110101596870877, 2.714942820864931328 ) ) ;
#95662=CARTESIAN_POINT ( 'NONE',  ( -8.633843874998758494, 20.65557450359631630, -1.500000000000002220 ) ) ;
#95665=CARTESIAN_POINT ( 'NONE',  ( -34.52287095715006160, -23.47596703998600631, 11.44779298504229459 ) ) ;
#95666=CARTESIAN_POINT ( 'NONE',  ( -128.6228709571500417, -29.50250243563736774, 8.947779886222132717 ) ) ;
#95667=CARTESIAN_POINT ( 'NONE',  ( -40.17059228844927787, -25.31544866396273363, 5.061091936170584837 ) ) ;
#95668=CARTESIAN_POINT ( 'NONE',  ( -125.5228709571500616, -23.48783264083375144, -1.443836473376139740 ) ) ;
#95669=CARTESIAN_POINT ( 'NONE',  ( -97.25031873460709164, -24.47917135695840685, 9.440663514584127114 ) ) ;
#95670=CARTESIAN_POINT ( 'NONE',  ( -19.52990877098713796, 1.257015143768854815, 11.49999999999998934 ) ) ;
#95671=CARTESIAN_POINT ( 'NONE',  ( -49.51538943686712457, -25.28145962008399650, 4.090414597456915935 ) ) ;
#95672=ORIENTED_EDGE ( 'NONE', *, *, #24448, .F. ) ;
#95673=CARTESIAN_POINT ( 'NONE',  ( 2.436486579176012413, 21.40072447632485364, 11.49999999999998934 ) ) ;
#95674=CARTESIAN_POINT ( 'NONE',  ( -128.5554938434827932, -24.51314013834317151, 0.6176544820404290537 ) ) ;
#95675=CARTESIAN_POINT ( 'NONE',  ( -81.01373513877602761, -25.30394778790603638, 5.057100112635003697 ) ) ;
#95676=CARTESIAN_POINT ( 'NONE',  ( -42.62287095715004881, -29.50250786944525672, 11.44777988621624232 ) ) ;
#95679=CARTESIAN_POINT ( 'NONE',  ( -14.98413761715186077, 17.36544542080599740, -1.500000000000002220 ) ) ;
#95681=PLANE ( 'NONE',  #62906 ) ;
#95682=CARTESIAN_POINT ( 'NONE',  ( -53.53251464419344074, -24.65952944569304250, 1.056160979905695463 ) ) ;
#95683=CARTESIAN_POINT ( 'NONE',  ( -10.05502934987021391, 17.38067806581081598, 11.49999999999999645 ) ) ;
#95684=DIRECTION ( 'NONE',  ( 0.000000000000000000, -2.173523156925980399E-06, 0.9999999999976378895 ) ) ;
#95685=CARTESIAN_POINT ( 'NONE',  ( -119.2228709571500644, -23.47593901973090169, -1.443836447538996426 ) ) ;
#95687=CARTESIAN_POINT ( 'NONE',  ( -65.62287095715011276, -24.51163499207176244, 0.6490370598554294768 ) ) ;
#95688=DIRECTION ( 'NONE',  ( -3.773278334453079618E-23, 0.9999999999976377785, 2.173523156925979975E-06 ) ) ;
#95689=CARTESIAN_POINT ( 'NONE',  ( -3.387584560642538101, 19.54024307811383210, 11.49999999999998934 ) ) ;
#95691=CARTESIAN_POINT ( 'NONE',  ( 15.15379598424239838, -12.58889634127381640, -1.500000000000002220 ) ) ;
#95694=CARTESIAN_POINT ( 'NONE',  ( -54.52287095715006870, -23.48786465467240347, 11.44779295918255002 ) ) ;
#95696=CARTESIAN_POINT ( 'NONE',  ( -115.6228709571499564, -24.51163499207178731, 0.6490370598555471604 ) ) ;
#95697=DIRECTION ( 'NONE',  ( 0.000000000000000000, -0.9999999999976377785, -2.173523156925979128E-06 ) ) ;
#95698=CARTESIAN_POINT ( 'NONE',  ( 20.58124611042576646, 0.8182449333618511123, 11.49999999999999645 ) ) ;
#95699=CARTESIAN_POINT ( 'NONE',  ( -128.5228709571500758, -23.96177878511310055, 10.65340807706329507 ) ) ;
#95700=AXIS2_PLACEMENT_3D ( 'NONE', #28389, #90296, #74083 ) ;
#95701=CARTESIAN_POINT ( 'NONE',  ( 20.74359285767136640, 8.971229656761206428, 11.49999999999999645 ) ) ;
#95703=LINE ( 'NONE', #33806, #7025 ) ;
#95704=CARTESIAN_POINT ( 'NONE',  ( -56.52287095715009002, -24.51283580621365132, 0.6167428607019713738 ) ) ;
#95705=EDGE_CURVE ( 'NONE', #33400, #61899, #50531, .T. ) ;
#95706=CARTESIAN_POINT ( 'NONE',  ( -39.62287095715005592, -23.72747288104441665, -1.053458166803662888 ) ) ;
#95707=EDGE_CURVE ( 'NONE', #15171, #41799, #14557, .T. ) ;
#95708=CARTESIAN_POINT ( 'NONE',  ( -27.26363273317966573, -24.61460103318581716, 8.203483245735846197 ) ) ;
#95710=CARTESIAN_POINT ( 'NONE',  ( -97.62287095715005592, -29.50247984919015209, -1.443849546365050029 ) ) ;
#95713=CARTESIAN_POINT ( 'NONE',  ( -79.64180909446726275, -25.26749935932355484, 5.241605752690947639 ) ) ;
#95714=CARTESIAN_POINT ( 'NONE',  ( 12.51456667378993259, 19.11410217522374921, 11.49999999999998934 ) ) ;
#95715=CARTESIAN_POINT ( 'NONE',  ( -105.6228709571500417, -24.99132157543166954, 2.256160258750667502 ) ) ;
#95716=CARTESIAN_POINT ( 'NONE',  ( -36.52287095715006870, -23.48783264082477018, -1.443836473390097019 ) ) ;
#95717=CARTESIAN_POINT ( 'NONE',  ( -63.58339596546591821, -24.51419770103158058, 9.386484678747173405 ) ) ;
#95718=CARTESIAN_POINT ( 'NONE',  ( 9.939345090160914609, -20.19931669485651682, 11.49999999999999645 ) ) ;
#95719=ORIENTED_EDGE ( 'NONE', *, *, #78118, .F. ) ;
#95721=CARTESIAN_POINT ( 'NONE',  ( 7.969717912702302343, -20.46423023992739942, 11.49999999999998934 ) ) ;
#95723=CARTESIAN_POINT ( 'NONE',  ( -44.56898981399523763, -23.48786465467240347, 11.44779295918255357 ) ) ;
#95724=CARTESIAN_POINT ( 'NONE',  ( -29.20082839157102583, -24.79699936332711729, 5.852070492749260389 ) ) ;
#95727=DIRECTION ( 'NONE',  ( -0.000000000000000000, 2.173523156925979552E-06, -0.9999999999976378895 ) ) ;
#95728=CARTESIAN_POINT ( 'NONE',  ( -107.5228709571501184, -23.95044443724992789, 10.65354141964649237 ) ) ;
#95730=CARTESIAN_POINT ( 'NONE',  ( -54.60549947881357014, -23.73791477778911130, 11.05961554403171299 ) ) ;
#95731=CARTESIAN_POINT ( 'NONE',  ( -2.888065500968368227, -20.30684875360264741, -1.500000000000002220 ) ) ;
#95732=ORIENTED_EDGE ( 'NONE', *, *, #9048, .F. ) ;
#95735=CARTESIAN_POINT ( 'NONE',  ( -50.24400751237210017, -25.31394886661938770, 5.202389599532529552 ) ) ;
#95736=CARTESIAN_POINT ( 'NONE',  ( 22.28998074345494729, -6.091270044117925053, -1.500000000000002220 ) ) ;
#95738=CARTESIAN_POINT ( 'NONE',  ( 18.28078834835902455, 8.925752885971231620, -1.500000000000002220 ) ) ;
#95739=VERTEX_POINT ( 'NONE', #42931 ) ;
#95740=DIRECTION ( 'NONE',  ( -3.773278334453079618E-23, 0.9999999999976377785, 2.173523156925979975E-06 ) ) ;
#95741=CARTESIAN_POINT ( 'NONE',  ( -50.38191529551148307, -25.12049752546737835, 2.832404795212222659 ) ) ;
#95742=PLANE ( 'NONE',  #27013 ) ;
#95743=CARTESIAN_POINT ( 'NONE',  ( -57.62287095715004881, -23.48783264082478794, -1.443836473390068820 ) ) ;
#95744=ORIENTED_EDGE ( 'NONE', *, *, #52988, .F. ) ;
#95745=CARTESIAN_POINT ( 'NONE',  ( -28.74075323809458737, -24.76880966510508486, 2.791733147577219132 ) ) ;
#95746=CARTESIAN_POINT ( 'NONE',  ( -49.69311491917191148, -25.26385837989523964, 4.912235144068747061 ) ) ;
#95747=ORIENTED_EDGE ( 'NONE', *, *, #61451, .T. ) ;
#95748=CARTESIAN_POINT ( 'NONE',  ( -9.565632364391108311, -18.43008791299702764, -1.500000000000002220 ) ) ;
#95750=ORIENTED_EDGE ( 'NONE', *, *, #36047, .T. ) ;
#95751=CARTESIAN_POINT ( 'NONE',  ( -125.5903909907711267, -24.15503026093915295, -0.2815557561904348804 ) ) ;
#95753=CARTESIAN_POINT ( 'NONE',  ( -41.56077783461210373, -23.73791477778911485, 11.05961554403170766 ) ) ;
#95754=CARTESIAN_POINT ( 'NONE',  ( -28.62287095715004881, -29.50248528299880846, 1.056150804693231082 ) ) ;
#95755=VERTEX_POINT ( 'NONE', #90089 ) ;
#95756=ORIENTED_EDGE ( 'NONE', *, *, #63140, .T. ) ;
#95758=CARTESIAN_POINT ( 'NONE',  ( -68.62287095715005592, -23.48786465467241058, 11.44779295918254647 ) ) ;
#95759=CARTESIAN_POINT ( 'NONE',  ( -27.70544111104076990, -24.61528742064533049, 1.628749860405701799 ) ) ;
#95760=CARTESIAN_POINT ( 'NONE',  ( -10.28628152547328511, -19.52461415289770130, 11.49999999999999645 ) ) ;
#95762=CARTESIAN_POINT ( 'NONE',  ( -103.5151658127220458, -24.15543982623907482, -0.2315651400026619011 ) ) ;
#95763=CARTESIAN_POINT ( 'NONE',  ( -9.785633969878258398, 20.35780147342342516, -1.500000000000002220 ) ) ;
#95764=EDGE_CURVE ( 'NONE', #53793, #36016, #35255, .T. ) ;
#95765=CARTESIAN_POINT ( 'NONE',  ( -90.62287095715004170, -23.48783264082478794, -1.443836473390063713 ) ) ;
#95766=VERTEX_POINT ( 'NONE', #58644 ) ;
#95769=VECTOR ( 'NONE', #76735, 1000.000000000000227 ) ;
#95770=CARTESIAN_POINT ( 'NONE',  ( -93.58953762381672448, -23.47593901973091235, -1.443836447539002865 ) ) ;
#95771=B_SPLINE_CURVE_WITH_KNOTS ( 'NONE', 3,
 ( #66817, #12502, #22094, #52073 ),
 .UNSPECIFIED., .F., .F.,
 ( 4, 4 ),
 ( 0.8010720259253786280, 0.8100784571974942727 ),
 .UNSPECIFIED. ) ;
#95773=B_SPLINE_CURVE_WITH_KNOTS ( 'NONE', 3,
 ( #40756, #73217, #94537, #25023 ),
 .UNSPECIFIED., .F., .F.,
 ( 4, 4 ),
 ( 0.000000000000000000, 9.999999999998206125E-05 ),
 .UNSPECIFIED. ) ;
#95774=PLANE ( 'NONE',  #27926 ) ;
#95776=CARTESIAN_POINT ( 'NONE',  ( -1.756177585742932479, 21.11346882147791959, 11.49999999999998934 ) ) ;
#95779=DIRECTION ( 'NONE',  ( 0.000000000000000000, 0.9999999999976377785, 2.173523156925979975E-06 ) ) ;
#95780=CARTESIAN_POINT ( 'NONE',  ( -9.187330254778467875, -20.22999604658808082, -1.500000000000002220 ) ) ;
#95785=CARTESIAN_POINT ( 'NONE',  ( -36.59393400239565608, -24.15620529776627379, 10.23563542870660825 ) ) ;
#95786=CARTESIAN_POINT ( 'NONE',  ( -49.62287095715005592, -24.66019654487199020, 8.947790411086135265 ) ) ;
#95787=CARTESIAN_POINT ( 'NONE',  ( 10.22484414329051994, 16.58839404647166660, 11.49999999999998934 ) ) ;
#95788=CARTESIAN_POINT ( 'NONE',  ( 11.41860910855227829, 18.14899599152127152, 11.49999999999998934 ) ) ;
#95789=CARTESIAN_POINT ( 'NONE',  ( -56.62287095715007013, -24.33832256527049154, 0.1851278514138594566 ) ) ;
#95790=CARTESIAN_POINT ( 'NONE',  ( -26.59970390766585169, -24.57999573590466014, 1.981117045598722370 ) ) ;
#95793=CARTESIAN_POINT ( 'NONE',  ( -7.854035805165779927, 21.33931789143995417, -1.500000000000002220 ) ) ;
#95795=CARTESIAN_POINT ( 'NONE',  ( -102.5508244618846163, -24.34968618360934656, 0.1864209137778959358 ) ) ;
#95796=CARTESIAN_POINT ( 'NONE',  ( -101.5895376238167245, -24.66019654487199375, 8.947790411086133489 ) ) ;
#95797=CARTESIAN_POINT ( 'NONE',  ( 19.88832268942539017, -0.5522253751840191516, 11.49999999999999645 ) ) ;
#95798=CARTESIAN_POINT ( 'NONE',  ( -104.5951184837940531, -23.73766607897670866, -1.055555164236450016 ) ) ;
#95799=DIRECTION ( 'NONE',  ( -3.773278334453079618E-23, 0.9999999999976377785, 2.173523156925979975E-06 ) ) ;
#95800=CARTESIAN_POINT ( 'NONE',  ( -48.48929744942994802, -24.51314013834315375, 0.6176544820404137326 ) ) ;
#95803=LINE ( 'NONE', #11073, #37735 ) ;
#95804=CARTESIAN_POINT ( 'NONE',  ( 18.84366469573077296, 10.75509914293975555, 11.49999999999998934 ) ) ;
#95805=CARTESIAN_POINT ( 'NONE',  ( -67.55620429048339304, -24.65952944569304961, 1.056160979905695685 ) ) ;
#95806=B_SPLINE_CURVE_WITH_KNOTS ( 'NONE', 3,
 ( #37782, #68736, #62128, #30666 ),
 .UNSPECIFIED., .F., .F.,
 ( 4, 4 ),
 ( 0.000000000000000000, 0.0001000000000000167422 ),
 .UNSPECIFIED. ) ;
#95807=CARTESIAN_POINT ( 'NONE',  ( -3.206006181753352724, -19.19236486397402430, -1.500000000000002220 ) ) ;
#95812=CARTESIAN_POINT ( 'NONE',  ( -19.05221060042639536, -7.346018566486852031, 11.49999999999999645 ) ) ;
#95817=CARTESIAN_POINT ( 'NONE',  ( -72.52287095715007581, -24.34917612406836795, 0.1852690917426531025 ) ) ;
#95819=CARTESIAN_POINT ( 'NONE',  ( -39.18717306657202215, -25.27985411147982120, 4.881706710394202453 ) ) ;
#95820=EDGE_CURVE ( 'NONE', #28727, #64178, #24273, .T. ) ;
#95821=PLANE ( 'NONE',  #27945 ) ;
#95822=DIRECTION ( 'NONE',  ( 0.000000000000000000, 0.9999999999976377785, 2.173523156925979975E-06 ) ) ;
#95826=EDGE_CURVE ( 'NONE', #38350, #11878, #65460, .T. ) ;
#95828=CARTESIAN_POINT ( 'NONE',  ( -19.06187107478486098, -12.82570580458313003, 11.49999999999999645 ) ) ;
#95829=CARTESIAN_POINT ( 'NONE',  ( 19.47892149737544187, 11.75266795981601753, 11.49999999999998934 ) ) ;
#95831=EDGE_CURVE ( 'NONE', #98210, #42298, #50879, .T. ) ;
#95832=LINE ( 'NONE', #26327, #39860 ) ;
#95833=CARTESIAN_POINT ( 'NONE',  ( -90.58449521732619303, -24.83618233451450763, 1.606449574219535492 ) ) ;
#95835=CARTESIAN_POINT ( 'NONE',  ( -125.5228709571500616, -23.47593901973090524, -1.443836447538996204 ) ) ;
#95837=CARTESIAN_POINT ( 'NONE',  ( -70.01777984349551787, -25.14013070378048198, 7.061429261598838991 ) ) ;
#95838=CARTESIAN_POINT ( 'NONE',  ( -11.18773875818744656, -18.78983145652188469, 11.49999999999998934 ) ) ;
#95840=B_SPLINE_CURVE_WITH_KNOTS ( 'NONE', 3,
 ( #4169, #37103, #58958, #20871, #35120, #68067 ),
 .UNSPECIFIED., .F., .F.,
 ( 4, 2, 4 ),
 ( 0.000000000000000000, 0.001380901958385388545, 0.002761803916770777089 ),
 .UNSPECIFIED. ) ;
#95841=CARTESIAN_POINT ( 'NONE',  ( -26.42866040157690222, -24.83930146701730735, 3.123068956510520966 ) ) ;
#95843=CARTESIAN_POINT ( 'NONE',  ( -81.58953762381673869, -23.47593901973091235, -1.443836447539004642 ) ) ;
#95844=ORIENTED_EDGE ( 'NONE', *, *, #52411, .T. ) ;
#95845=B_SPLINE_CURVE_WITH_KNOTS ( 'NONE', 3,
 ( #12448, #66268, #13940, #97191, #28183, #89583, #29672, #58636 ),
 .UNSPECIFIED., .F., .F.,
 ( 4, 2, 2, 4 ),
 ( -0.001240355328176661687, -0.0002398155169397982525, 0.0007607242942970651820, 0.002761803916770787931 ),
 .UNSPECIFIED. ) ;
#95846=CARTESIAN_POINT ( 'NONE',  ( -15.55180764702766716, 13.24544322234432414, 11.49999999999998934 ) ) ;
#95848=ORIENTED_EDGE ( 'NONE', *, *, #6354, .T. ) ;
#95850=CARTESIAN_POINT ( 'NONE',  ( 8.869223403490039459, -21.23658630136709391, -1.500000000000002220 ) ) ;
#95851=DIRECTION ( 'NONE',  ( -3.773278334453079618E-23, 0.9999999999976377785, 2.173523156925979975E-06 ) ) ;
#95852=ORIENTED_EDGE ( 'NONE', *, *, #19224, .F. ) ;
#95853=CARTESIAN_POINT ( 'NONE',  ( -124.6228709571500701, -24.66019654487200086, 8.947790411086121054 ) ) ;
#95854=CARTESIAN_POINT ( 'NONE',  ( -101.6228709571500559, -23.48783264082479505, -1.443836473390062380 ) ) ;
#95857=CARTESIAN_POINT ( 'NONE',  ( 12.64048258313813733, 17.25876517447949610, 11.49999999999999645 ) ) ;
#95858=ORIENTED_EDGE ( 'NONE', *, *, #28287, .T. ) ;
#95859=ORIENTED_EDGE ( 'NONE', *, *, #88775, .T. ) ;
#95860=CARTESIAN_POINT ( 'NONE',  ( -21.98633505697190671, -3.258044352128648846, 11.49999999999998934 ) ) ;
#95861=CARTESIAN_POINT ( 'NONE',  ( 16.58470376584361361, 12.37529123428901556, -1.500000000000002220 ) ) ;
#95863=CARTESIAN_POINT ( 'NONE',  ( -115.6228709571500559, -29.50247984919015209, -1.443849546365046699 ) ) ;
#95867=CARTESIAN_POINT ( 'NONE',  ( -122.6228709571500417, -29.50248528299804818, 1.056150453629045360 ) ) ;
#95869=CARTESIAN_POINT ( 'NONE',  ( -50.38191529551148307, -25.10935127036004033, 2.832404819438866017 ) ) ;
#95870=CARTESIAN_POINT ( 'NONE',  ( 16.20321855003292555, -13.12800272717607619, -1.500000000000002220 ) ) ;
#95871=CARTESIAN_POINT ( 'NONE',  ( 21.88901064076550185, 0.7357440816682787599, 11.49999999999999645 ) ) ;
#95873=CARTESIAN_POINT ( 'NONE',  ( -107.6228709571500843, -24.51387760970725083, 9.387446482453409402 ) ) ;
#95874=CARTESIAN_POINT ( 'NONE',  ( -61.24303308397303880, -25.03284409833926105, 7.563174216509380265 ) ) ;
#95875=CARTESIAN_POINT ( 'NONE',  ( 16.80569330386292748, 14.95695114220347932, -1.500000000000002220 ) ) ;
#95876=CARTESIAN_POINT ( 'NONE',  ( 11.32296221242833667, -17.63459971646239310, 11.49999999999998934 ) ) ;
#95877=CARTESIAN_POINT ( 'NONE',  ( -26.09849696787948403, -24.97066838479807416, 5.165052413643238083 ) ) ;
#95879=CARTESIAN_POINT ( 'NONE',  ( -53.52287095715006870, -24.64898659630367916, 1.056161002820821038 ) ) ;
#95880=CARTESIAN_POINT ( 'NONE',  ( -88.62287095715004170, -23.47593901973091235, -1.443836447539002865 ) ) ;
#95885=LINE ( 'NONE', #12138, #88723 ) ;
#95887=CARTESIAN_POINT ( 'NONE',  ( 2.169945595249806125, 21.32849103866527329, -1.500000000000002220 ) ) ;
#95889=ORIENTED_EDGE ( 'NONE', *, *, #12141, .T. ) ;
#95891=CARTESIAN_POINT ( 'NONE',  ( 7.532573551308565207, 19.69859070278346991, 11.49999999999998934 ) ) ;
#95892=CARTESIAN_POINT ( 'NONE',  ( -61.55620429048340014, -23.47593901973091235, -1.443836447539007972 ) ) ;
#95895=CARTESIAN_POINT ( 'NONE',  ( -117.5228709571500758, -23.48783264082477729, -1.443836473390083697 ) ) ;
#95897=CARTESIAN_POINT ( 'NONE',  ( 9.306852550357104903, -20.00191182576189064, -1.500000000000002220 ) ) ;
#95898=ORIENTED_EDGE ( 'NONE', *, *, #2962, .T. ) ;
#95899=CARTESIAN_POINT ( 'NONE',  ( -65.59839509469505003, -24.15602025860896518, 10.28564288303535257 ) ) ;
#95900=EDGE_CURVE ( 'NONE', #6944, #21327, #63146, .T. ) ;
#95901=DIRECTION ( 'NONE',  ( 0.000000000000000000, -2.173523156925980399E-06, 0.9999999999976378895 ) ) ;
#95903=CARTESIAN_POINT ( 'NONE',  ( -62.49489557338270629, -24.51419770103156281, 9.386484678747184063 ) ) ;
#95904=B_SPLINE_CURVE_WITH_KNOTS ( 'NONE', 3,
 ( #303, #63220, #31247, #62218, #93138, #23621 ),
 .UNSPECIFIED., .F., .F.,
 ( 4, 2, 4 ),
 ( 1.570887131795413739E-05, 0.001396322306279768229, 0.002776935741241582344 ),
 .UNSPECIFIED. ) ;
#95905=VECTOR ( 'NONE', #27040, 1000.000000000000114 ) ;
#95906=PLANE ( 'NONE',  #94305 ) ;
#95909=CARTESIAN_POINT ( 'NONE',  ( 20.65877813657638740, 5.380652674160894655, -1.500000000000002220 ) ) ;
#95910=CARTESIAN_POINT ( 'NONE',  ( -104.5228709571500332, -24.35013146730204525, 9.818937971375099494 ) ) ;
#95911=DIRECTION ( 'NONE',  ( -3.773278334453079030E-23, 0.9999999999976377785, 2.173523156925979128E-06 ) ) ;
#95912=CARTESIAN_POINT ( 'NONE',  ( -64.65372345458705183, -23.48786465467241058, 11.44779295918254824 ) ) ;
#95913=DIRECTION ( 'NONE',  ( -3.773278334453079618E-23, 0.9999999999976377785, 2.173523156925979975E-06 ) ) ;
#95915=CARTESIAN_POINT ( 'NONE',  ( 20.50669422456317292, -9.396423750077818937, -1.500000000000002220 ) ) ;
#95917=ORIENTED_EDGE ( 'NONE', *, *, #1703, .F. ) ;
#95919=CARTESIAN_POINT ( 'NONE',  ( -31.57476609544196933, -24.66019654487199020, 8.947790411086133489 ) ) ;
#95920=CARTESIAN_POINT ( 'NONE',  ( 15.33752688427012778, 12.42672799324400934, 11.49999999999999645 ) ) ;
#95921=CARTESIAN_POINT ( 'NONE',  ( -40.62287095715005592, -23.47593901973091235, -1.443836447539011525 ) ) ;
#95922=CARTESIAN_POINT ( 'NONE',  ( -67.55938042207226601, -23.73766607897670511, -1.055555164236457788 ) ) ;
#95923=B_SPLINE_CURVE_WITH_KNOTS ( 'NONE', 3,
 ( #47309, #24958, #77727, #25461 ),
 .UNSPECIFIED., .F., .F.,
 ( 4, 4 ),
 ( 0.5791858693580937967, 0.5801866163988591563 ),
 .UNSPECIFIED. ) ;
#95926=CARTESIAN_POINT ( 'NONE',  ( -99.62287095715004170, -24.66019654487199730, 8.947790411086122830 ) ) ;
#95928=CARTESIAN_POINT ( 'NONE',  ( -20.99440926880444636, 4.982473936180791263, -1.500000000000002220 ) ) ;
#95929=CARTESIAN_POINT ( 'NONE',  ( -71.52287095715007581, -23.47596703998600631, 11.44779298504228748 ) ) ;
#95931=CARTESIAN_POINT ( 'NONE',  ( -68.62287095715005592, -24.64965695001468404, 8.947790433994184056 ) ) ;
#95932=CARTESIAN_POINT ( 'NONE',  ( -97.62287095715005592, -29.50248528299804818, 1.056150453629042030 ) ) ;
#95933=CARTESIAN_POINT ( 'NONE',  ( -19.30086548479123465, -4.275078920326023990, -1.500000000000002220 ) ) ;
#95934=ORIENTED_EDGE ( 'NONE', *, *, #6030, .T. ) ;
#95935=CARTESIAN_POINT ( 'NONE',  ( 9.670762957215185196, 17.83519281925787325, 11.49999999999999645 ) ) ;
#95937=VECTOR ( 'NONE', #18146, 1000.000000000000114 ) ;
#95938=VERTEX_POINT ( 'NONE', #61649 ) ;
#95939=CARTESIAN_POINT ( 'NONE',  ( -46.52287095715006160, -23.47596703998600631, 11.44779298504229104 ) ) ;
#95940=DIRECTION ( 'NONE',  ( -3.773278334453080206E-23, 0.9999999999976377785, 2.173523156925979975E-06 ) ) ;
#95942=CARTESIAN_POINT ( 'NONE',  ( -69.86226356453386188, -25.11033435731149055, 2.832404375966413479 ) ) ;
#95943=DIRECTION ( 'NONE',  ( 0.000000000000000000, 0.9999999999976377785, 2.173523156925979975E-06 ) ) ;
#95944=CARTESIAN_POINT ( 'NONE',  ( -32.68833172073793492, -25.11010177982458913, 2.831122766525575152 ) ) ;
#95945=CARTESIAN_POINT ( 'NONE',  ( 15.05167116458888010, 13.23127732593390959, -1.500000000000002220 ) ) ;
#95946=EDGE_CURVE ( 'NONE', #95739, #16907, #17079, .T. ) ;
#95949=CARTESIAN_POINT ( 'NONE',  ( -51.52287095715006870, -24.65952944569304606, 1.056160979905693686 ) ) ;
#95952=CARTESIAN_POINT ( 'NONE',  ( -35.57730181162962424, -24.83618233451448987, 1.606449574219547261 ) ) ;
#95953=CARTESIAN_POINT ( 'NONE',  ( -52.52287095715006870, -24.64898659630367916, 1.056161002820821038 ) ) ;
#95954=AXIS2_PLACEMENT_3D ( 'NONE', #71114, #45766, #32543 ) ;
#95955=EDGE_CURVE ( 'NONE', #10587, #77573, #42442, .T. ) ;
#95956=CARTESIAN_POINT ( 'NONE',  ( -105.5228709571500616, -24.51163499207175178, 0.6490370598554284776 ) ) ;
#95958=B_SPLINE_CURVE_WITH_KNOTS ( 'NONE', 3,
 ( #98629, #4805, #27143, #97639 ),
 .UNSPECIFIED., .F., .F.,
 ( 4, 4 ),
 ( 0.000000000000000000, 9.999999999998897304E-05 ),
 .UNSPECIFIED. ) ;
#95961=DIRECTION ( 'NONE',  ( -1.000000000000000000, -3.773278334444166432E-23, -8.201307841325785021E-29 ) ) ;
#95963=CARTESIAN_POINT ( 'NONE',  ( -19.79944955726156763, -4.570829099900970860, 11.49999999999998934 ) ) ;
#95965=EDGE_CURVE ( 'NONE', #14117, #74994, #89699, .T. ) ;
#95967=CARTESIAN_POINT ( 'NONE',  ( -118.5895376238167387, -23.47596703998600631, 11.44779298504227683 ) ) ;
#95968=ORIENTED_EDGE ( 'NONE', *, *, #39225, .T. ) ;
#95969=CARTESIAN_POINT ( 'NONE',  ( -59.58301786718180892, -24.51419770103156281, 9.386484678747184063 ) ) ;
#95970=CARTESIAN_POINT ( 'NONE',  ( -49.39546678031889826, -25.12215307982809875, 6.587942430398275206 ) ) ;
#95971=VECTOR ( 'NONE', #36126, 1000.000000000000227 ) ;
#95972=CARTESIAN_POINT ( 'NONE',  ( -30.47287095715007865, -24.48778984439529793, 0.5888598878604692777 ) ) ;
#95973=CARTESIAN_POINT ( 'NONE',  ( -10.79823215447539653, -18.26288818932900071, 11.49999999999999645 ) ) ;
#95975=CARTESIAN_POINT ( 'NONE',  ( -17.14978611337857473, 13.99085498846200437, 11.49999999999998934 ) ) ;
#95976=CARTESIAN_POINT ( 'NONE',  ( 14.30100545221680441, -14.83292283143518375, -1.500000000000002220 ) ) ;
#95978=CARTESIAN_POINT ( 'NONE',  ( -41.50561517559466296, -23.96119346886880663, -0.6495511937831991434 ) ) ;
#95980=CARTESIAN_POINT ( 'NONE',  ( -54.65829041126421117, -23.48783264082476308, -1.443836473390098130 ) ) ;
#95981=DIRECTION ( 'NONE',  ( 0.000000000000000000, -0.9999999999976377785, -2.173523156925979128E-06 ) ) ;
#95982=ORIENTED_EDGE ( 'NONE', *, *, #71850, .F. ) ;
#95983=ORIENTED_EDGE ( 'NONE', *, *, #87134, .F. ) ;
#95987=DIRECTION ( 'NONE',  ( 0.000000000000000000, -2.173523156925979552E-06, 0.9999999999976378895 ) ) ;
#95988=LINE ( 'NONE', #57450, #1750 ) ;
#95989=CARTESIAN_POINT ( 'NONE',  ( 2.909938941155331360, -20.50406750007545398, -1.500000000000002220 ) ) ;
#95991=CARTESIAN_POINT ( 'NONE',  ( -2.129050106866105185, 21.58297100922832357, 11.49999999999999645 ) ) ;
#95992=ORIENTED_EDGE ( 'NONE', *, *, #58768, .T. ) ;
#95993=CARTESIAN_POINT ( 'NONE',  ( -69.86226847989213695, -25.12049686670126292, 2.832401160916445004 ) ) ;
#95994=CARTESIAN_POINT ( 'NONE',  ( -28.58953762381671737, -23.32893085120693044, 11.44779297967261478 ) ) ;
#95995=CARTESIAN_POINT ( 'NONE',  ( 12.67250375155129127, 18.46511205475877304, -1.500000000000002220 ) ) ;
#95996=B_SPLINE_CURVE_WITH_KNOTS ( 'NONE', 3,
 ( #39408, #31800, #62768, #93686, #55149, #86078 ),
 .UNSPECIFIED., .F., .F.,
 ( 4, 2, 4 ),
 ( 1.570887131794952276E-05, 0.001396322306279762808, 0.002776935741241575838 ),
 .UNSPECIFIED. ) ;
#95998=CARTESIAN_POINT ( 'NONE',  ( -71.62287095715005592, -23.48783264082478084, -1.443836473390067487 ) ) ;
#95999=EDGE_CURVE ( 'NONE', #97756, #33587, #84826, .T. ) ;
#96001=CARTESIAN_POINT ( 'NONE',  ( -121.5228709571500616, -23.48786465467241769, 11.44779295918253759 ) ) ;
#96002=FACE_OUTER_BOUND ( 'NONE', #65319, .T. ) ;
#96003=B_SPLINE_SURFACE_WITH_KNOTS ( 'NONE', 3, 3, ( 
 ( #95980, #49830, #26966, #10240 ),
 ( #19351, #64562, #73646, #24960 ),
 ( #48316, #25967, #79243, #2150 ),
 ( #65562, #42221, #50317, #17859 ),
 ( #72156, #33083, #73154, #3644 ),
 ( #64062, #48823, #57443, #34590 ),
 ( #3151, #94974, #96477, #88879 ) ),
 .UNSPECIFIED., .F., .F., .F.,
 ( 4, 3, 4 ),
 ( 4, 4 ),
 ( 0.0004766839783814135812, 0.1029713700210890814, 0.2054660560637967537 ),
 ( 0.7596872487054024958, 0.7610504915621147948 ),
 .UNSPECIFIED. ) ;
#96007=EDGE_LOOP ( 'NONE', ( #10400, #97968, #14319, #33567 ) ) ;
#96008=ADVANCED_FACE ( 'NONE', ( #11345 ), #48415, .F. ) ;
#96009=AXIS2_PLACEMENT_3D ( 'NONE', #1328, #69328, #78928 ) ;
#96010=CARTESIAN_POINT ( 'NONE',  ( -19.98547761299008130, 7.154247560337752887, -1.500000000000002220 ) ) ;
#96012=CARTESIAN_POINT ( 'NONE',  ( -88.50298424756591942, -24.65952944569304606, 1.056160979905701902 ) ) ;
#96013=CARTESIAN_POINT ( 'NONE',  ( 8.176594470695947692, -20.27425322898990601, 11.49999999999998934 ) ) ;
#96014=CARTESIAN_POINT ( 'NONE',  ( -103.5929781363113591, -23.96169478059713498, 10.65365249895717881 ) ) ;
#96016=FACE_OUTER_BOUND ( 'NONE', #51813, .T. ) ;
#96017=CARTESIAN_POINT ( 'NONE',  ( 12.52028139621776326, 17.89958603277719718, -1.500000000000002220 ) ) ;
#96022=ORIENTED_EDGE ( 'NONE', *, *, #57037, .T. ) ;
#96023=CARTESIAN_POINT ( 'NONE',  ( -30.58316948069863628, -25.14456584033169051, 2.729964928219756004 ) ) ;
#96024=VERTEX_POINT ( 'NONE', #26066 ) ;
#96025=VECTOR ( 'NONE', #36779, 1000.000000000000114 ) ;
#96027=CARTESIAN_POINT ( 'NONE',  ( -82.50023227949210991, -24.65952944569304606, 1.056160979905703012 ) ) ;
#96028=CARTESIAN_POINT ( 'NONE',  ( -1.624102159174229731, 21.17438964843747584, 11.49999999999998934 ) ) ;
#96030=CARTESIAN_POINT ( 'NONE',  ( -30.63208233338743725, -23.87624887660336981, 11.01174216661999594 ) ) ;
#96033=CARTESIAN_POINT ( 'NONE',  ( -68.65187207870859254, -23.48783264082476308, -1.443836473390094799 ) ) ;
#96034=EDGE_CURVE ( 'NONE', #89278, #21561, #15814, .T. ) ;
#96035=CARTESIAN_POINT ( 'NONE',  ( -16.37229413335033001, -10.43475415037859655, 11.49999999999998934 ) ) ;
#96037=ORIENTED_EDGE ( 'NONE', *, *, #69523, .F. ) ;
#96038=CARTESIAN_POINT ( 'NONE',  ( 14.28107258077893604, -13.35224110012613963, 11.49999999999999645 ) ) ;
#96041=ORIENTED_EDGE ( 'NONE', *, *, #97731, .F. ) ;
#96042=CARTESIAN_POINT ( 'NONE',  ( -97.52287095715009002, -23.73907113216990084, -1.053371485793246576 ) ) ;
#96043=ADVANCED_FACE ( 'NONE', ( #63652 ), #26577, .T. ) ;
#96044=DIRECTION ( 'NONE',  ( -3.773278334453079618E-23, 0.9999999999976377785, 2.173523156925979975E-06 ) ) ;
#96045=EDGE_CURVE ( 'NONE', #39879, #79654, #1276, .T. ) ;
#96047=VECTOR ( 'NONE', #91304, 1000.000000000000114 ) ;
#96048=CARTESIAN_POINT ( 'NONE',  ( -81.34205133964172774, -25.24813932869157540, 7.294265035158486121 ) ) ;
#96049=CARTESIAN_POINT ( 'NONE',  ( -3.718233408413001762, 19.32670252783854536, -1.500000000000002220 ) ) ;
#96052=ORIENTED_EDGE ( 'NONE', *, *, #86793, .T. ) ;
#96053=LINE ( 'NONE', #40763, #42405 ) ;
#96055=B_SPLINE_CURVE_WITH_KNOTS ( 'NONE', 3,
 ( #62555, #9251, #93479, #79260, #23972, #54942, #85883, #47328 ),
 .UNSPECIFIED., .F., .F.,
 ( 4, 2, 2, 4 ),
 ( 0.000000000000000000, 0.002001079623178226262, 0.003001619434767339393, 0.004002159246356452524 ),
 .UNSPECIFIED. ) ;
#96058=ORIENTED_EDGE ( 'NONE', *, *, #23875, .F. ) ;
#96060=CARTESIAN_POINT ( 'NONE',  ( -59.92287095715006728, -23.47596703998600276, 11.44779298504227860 ) ) ;
#96061=CARTESIAN_POINT ( 'NONE',  ( -52.62287095715005592, -23.47593901973091235, -1.443836447539009749 ) ) ;
#96062=CARTESIAN_POINT ( 'NONE',  ( -97.58474207598447947, -24.66019654487199730, 8.947790411086115725 ) ) ;
#96064=CARTESIAN_POINT ( 'NONE',  ( -69.57050707393172218, -25.31201661394681324, 5.639419279061749890 ) ) ;
#96065=AXIS2_PLACEMENT_3D ( 'NONE', #37493, #28882, #89787 ) ;
#96066=CARTESIAN_POINT ( 'NONE',  ( -114.5222273195970075, -23.48786465467241413, 11.44779295918253581 ) ) ;
#96067=CARTESIAN_POINT ( 'NONE',  ( 6.088051586893210576, -19.00464151315268424, 11.49999999999998934 ) ) ;
#96069=CARTESIAN_POINT ( 'NONE',  ( -75.62366547609374834, -25.00182538069147142, 7.747789668545045139 ) ) ;
#96070=CARTESIAN_POINT ( 'NONE',  ( -18.24115112668064853, 7.888873183027880209, -1.500000000000002220 ) ) ;
#96071=ORIENTED_EDGE ( 'NONE', *, *, #61711, .F. ) ;
#96072=CARTESIAN_POINT ( 'NONE',  ( -28.62287095715006302, -23.33147402473456822, -1.443835808584760683 ) ) ;
#96073=CARTESIAN_POINT ( 'NONE',  ( -104.6228709571500133, -24.33927499327854704, 9.819080762295815390 ) ) ;
#96076=CARTESIAN_POINT ( 'NONE',  ( -12.40256906124370673, -16.71776976679197801, 11.49999999999999645 ) ) ;
#96077=CARTESIAN_POINT ( 'NONE',  ( -35.62287095715005592, -23.47593901973091235, -1.443836447539011525 ) ) ;
#96078=B_SPLINE_CURVE_WITH_KNOTS ( 'NONE', 3,
 ( #90118, #73407, #81012, #36334, #12492, #89126 ),
 .UNSPECIFIED., .F., .F.,
 ( 4, 2, 4 ),
 ( 0.000000000000000000, 0.001380764517854769302, 0.002761529035709538605 ),
 .UNSPECIFIED. ) ;
#96079=EDGE_CURVE ( 'NONE', #3121, #86407, #81062, .T. ) ;
#96080=CARTESIAN_POINT ( 'NONE',  ( -60.52287095715006160, -23.47593901973090169, -1.443836447538996870 ) ) ;
#96081=CARTESIAN_POINT ( 'NONE',  ( -15.12447472116105729, 17.10960193589383849, 11.49999999999999645 ) ) ;
#96085=CARTESIAN_POINT ( 'NONE',  ( -62.62287095715002039, -23.94994826722515313, -0.6494450866351701990 ) ) ;
#96086=EDGE_CURVE ( 'NONE', #6944, #72067, #15631, .T. ) ;
#96089=CARTESIAN_POINT ( 'NONE',  ( 12.15850541088210868, 16.18036119754114566, 11.49999999999998934 ) ) ;
#96090=CARTESIAN_POINT ( 'NONE',  ( -106.5228709571500332, -24.51387760970726148, 9.387446482453402297 ) ) ;
#96091=ADVANCED_FACE ( 'NONE', ( #80859 ), #17450, .T. ) ;
#96092=DIRECTION ( 'NONE',  ( -0.000000000000000000, 2.173523156925979552E-06, -0.9999999999976378895 ) ) ;
#96094=EDGE_CURVE ( 'NONE', #5560, #8268, #2244, .T. ) ;
#96096=ORIENTED_EDGE ( 'NONE', *, *, #12415, .F. ) ;
#96097=CARTESIAN_POINT ( 'NONE',  ( -109.6228709571500559, -24.64965695001469115, 8.947790433994176951 ) ) ;
#96099=CARTESIAN_POINT ( 'NONE',  ( 19.63333621495807435, 3.783328549194958867, -1.500000000000002220 ) ) ;
#96101=CARTESIAN_POINT ( 'NONE',  ( -5.787726610425443674, -20.20099407548119075, 11.49999999999999645 ) ) ;
#96104=CARTESIAN_POINT ( 'NONE',  ( -0.5447568859041533873, -22.05808898580190558, 11.49999999999998934 ) ) ;
#96105=CARTESIAN_POINT ( 'NONE',  ( -40.38104457131870362, -25.27806106493511251, 5.081426816473861408 ) ) ;
#96106=ORIENTED_EDGE ( 'NONE', *, *, #57726, .F. ) ;
#96107=PLANE ( 'NONE',  #98638 ) ;
#96109=CARTESIAN_POINT ( 'NONE',  ( -72.59232901061996301, -24.15543982623907127, -0.2315651400026661755 ) ) ;
#96112=ORIENTED_EDGE ( 'NONE', *, *, #92591, .F. ) ;
#96114=CARTESIAN_POINT ( 'NONE',  ( -100.7878122855614293, -25.10935811319381372, 2.873140115367836867 ) ) ;
#96115=FACE_OUTER_BOUND ( 'NONE', #82511, .T. ) ;
#96116=CARTESIAN_POINT ( 'NONE',  ( -4.863915844574979275, 19.94883092034378791, -1.500000000000002220 ) ) ;
#96117=ORIENTED_EDGE ( 'NONE', *, *, #11760, .F. ) ;
#96120=LINE ( 'NONE', #17991, #99889 ) ;
#96121=CARTESIAN_POINT ( 'NONE',  ( 19.83320176327591255, -10.20924650237717835, 11.49999999999998934 ) ) ;
#96123=CARTESIAN_POINT ( 'NONE',  ( -114.6228709571500559, -29.50250243563736774, 8.947779886222136270 ) ) ;
#96128=CARTESIAN_POINT ( 'NONE',  ( -96.62287095715005592, -23.48786465467241413, 11.44779295918254114 ) ) ;
#96130=CARTESIAN_POINT ( 'NONE',  ( 20.80141654084381386, -1.409215765453083469, -1.500000000000002220 ) ) ;
#96131=EDGE_LOOP ( 'NONE', ( #2013, #14864, #30958, #41885 ) ) ;
#96136=ADVANCED_FACE ( 'NONE', ( #95081 ), #22618, .T. ) ;
#96137=CARTESIAN_POINT ( 'NONE',  ( -69.21490423241783674, -25.03149257829292651, 7.033986958848029047 ) ) ;
#96138=CARTESIAN_POINT ( 'NONE',  ( -19.04630365209304799, -9.011775662611203330, -1.500000000000002220 ) ) ;
#96142=DIRECTION ( 'NONE',  ( 0.000000000000000000, -0.9999999999976377785, -2.173523156925979975E-06 ) ) ;
#96143=AXIS2_PLACEMENT_3D ( 'NONE', #25384, #80175, #96397 ) ;
#96144=CARTESIAN_POINT ( 'NONE',  ( -101.3347705957103528, -25.03152393472591797, 7.306917963305517461 ) ) ;
#96145=CARTESIAN_POINT ( 'NONE',  ( -83.92287095715005307, -23.47593901973090169, -1.443836447538996870 ) ) ;
#96146=CARTESIAN_POINT ( 'NONE',  ( -17.53059066697263546, 12.75712217820542627, -1.500000000000002220 ) ) ;
#96147=CARTESIAN_POINT ( 'NONE',  ( -80.72310326078591913, -25.24759799559129192, 7.076933208677574250 ) ) ;
#96148=CARTESIAN_POINT ( 'NONE',  ( 22.20168578472828358, 1.497490109320031682, 11.49999999999999645 ) ) ;
#96150=CARTESIAN_POINT ( 'NONE',  ( -50.49683564601712504, -25.24728724001002433, 5.199897385844055364 ) ) ;
#96153=ORIENTED_EDGE ( 'NONE', *, *, #25796, .F. ) ;
#96154=CARTESIAN_POINT ( 'NONE',  ( -35.62287095715005592, -23.47596703998600276, 11.44779298504227505 ) ) ;
#96158=ADVANCED_FACE ( 'NONE', ( #83339 ), #82346, .F. ) ;
#96159=CARTESIAN_POINT ( 'NONE',  ( -87.52287095715006160, -23.72773821059536914, 11.05748984161097503 ) ) ;
#96160=CARTESIAN_POINT ( 'NONE',  ( -46.52287095715006160, -29.50250243563736774, 8.947779886222146928 ) ) ;
#96161=VERTEX_POINT ( 'NONE', #81853 ) ;
#96162=CARTESIAN_POINT ( 'NONE',  ( -130.5728709571500872, -24.71514176503767146, 0.9371183705310238699 ) ) ;
#96163=CARTESIAN_POINT ( 'NONE',  ( 6.649717926671450563, 21.43536518531312396, -1.500000000000002220 ) ) ;
#96164=ORIENTED_EDGE ( 'NONE', *, *, #61593, .F. ) ;
#96165=CARTESIAN_POINT ( 'NONE',  ( -112.5175246721842655, -24.15620529776628445, 10.23563542870659404 ) ) ;
#96169=EDGE_CURVE ( 'NONE', #71152, #69536, #35187, .T. ) ;
#96170=EDGE_CURVE ( 'NONE', #39801, #20337, #37174, .T. ) ;
#96171=LINE ( 'NONE', #10422, #91893 ) ;
#96173=CARTESIAN_POINT ( 'NONE',  ( -130.5728709571501156, -25.30557784678704891, 3.856996771331004048 ) ) ;
#96174=CARTESIAN_POINT ( 'NONE',  ( 3.881049643139886207, -19.21785841795820104, -1.500000000000002220 ) ) ;
#96177=VERTEX_POINT ( 'NONE', #96572 ) ;
#96178=ADVANCED_FACE ( 'NONE', ( #27073 ), #27577, .T. ) ;
#96179=CARTESIAN_POINT ( 'NONE',  ( 8.792760106793807040, 19.66521392739144858, -1.500000000000002220 ) ) ;
#96181=CARTESIAN_POINT ( 'NONE',  ( -70.94546041667526026, -25.25639558167272725, 6.902322488783775079 ) ) ;
#96182=LINE ( 'NONE', #95676, #27966 ) ;
#96184=CARTESIAN_POINT ( 'NONE',  ( 2.319610639010541764, -22.79860127089448696, -1.500000000000002220 ) ) ;
#96186=CARTESIAN_POINT ( 'NONE',  ( -66.52287095715007581, -23.47593901973090524, -1.443836447538997092 ) ) ;
#96187=CARTESIAN_POINT ( 'NONE',  ( -53.49620482326537285, -24.34968618360933590, 0.1864209137778785885 ) ) ;
#96188=CARTESIAN_POINT ( 'NONE',  ( -20.04763853020464737, 0.9818187932333496404, 11.49999999999999645 ) ) ;
#96189=CARTESIAN_POINT ( 'NONE',  ( -40.58953762381671737, -25.00182538069145011, 7.747789668545099317 ) ) ;
#96192=CARTESIAN_POINT ( 'NONE',  ( -102.5895376238167103, -24.64898659630368272, 1.056161002820388273 ) ) ;
#96195=CARTESIAN_POINT ( 'NONE',  ( 11.68167410197319001, -16.05257874518773065, -1.500000000000002220 ) ) ;
#96197=CARTESIAN_POINT ( 'NONE',  ( -90.62287095715004170, -24.92604778743018201, 8.074972756849357225 ) ) ;
#96198=CARTESIAN_POINT ( 'NONE',  ( -5.312243195520525596, -18.98051080891723430, -1.500000000000002220 ) ) ;
#96199=CARTESIAN_POINT ( 'NONE',  ( -42.52203047475234854, -23.48783264082477373, -1.443836473390076147 ) ) ;
#96200=B_SPLINE_CURVE_WITH_KNOTS ( 'NONE', 3,
 ( #5876, #75378, #82008, #59683, #90615, #28218 ),
 .UNSPECIFIED., .F., .F.,
 ( 4, 2, 4 ),
 ( 6.384118678617699402E-06, 0.001386860460828380406, 0.002767336802978143193 ),
 .UNSPECIFIED. ) ;
#96203=CARTESIAN_POINT ( 'NONE',  ( -115.6228709571500701, -24.91544648472627088, 1.928969306349434643 ) ) ;
#96205=CARTESIAN_POINT ( 'NONE',  ( -3.146292006899429783, -20.37002610441940220, 11.49999999999999645 ) ) ;
#96206=EDGE_CURVE ( 'NONE', #95483, #79654, #54904, .T. ) ;
#96207=CARTESIAN_POINT ( 'NONE',  ( -29.62287095715005592, -23.40871900810292772, -1.443836166241315055 ) ) ;
#96209=CARTESIAN_POINT ( 'NONE',  ( 20.84710439121840864, 8.857176948214046774, 11.49999999999999645 ) ) ;
#96210=EDGE_LOOP ( 'NONE', ( #6836, #26259, #4621, #92859 ) ) ;
#96211=CARTESIAN_POINT ( 'NONE',  ( -69.63000454671555417, -25.25639544928042568, 6.841411100453155036 ) ) ;
#96212=CARTESIAN_POINT ( 'NONE',  ( -97.52218086169804678, -23.48783264082477729, -1.443836473390088138 ) ) ;
#96213=AXIS2_PLACEMENT_3D ( 'NONE', #99006, #90415, #68579 ) ;
#96215=ADVANCED_FACE ( 'NONE', ( #91951 ), #23419, .F. ) ;
#96216=CARTESIAN_POINT ( 'NONE',  ( -76.62287095715007013, -29.50248528299804818, 1.056150453629038477 ) ) ;
#96219=CARTESIAN_POINT ( 'NONE',  ( -30.54627711375826493, -23.48004750822538611, -1.443836485791523128 ) ) ;
#96220=CARTESIAN_POINT ( 'NONE',  ( 20.53691900564983186, 10.01969956684014207, -1.500000000000002220 ) ) ;
#96221=DIRECTION ( 'NONE',  ( -0.000000000000000000, 2.173523156925979552E-06, -0.9999999999976378895 ) ) ;
#96222=ADVANCED_FACE ( 'NONE', ( #53408 ), #31047, .T. ) ;
#96223=CARTESIAN_POINT ( 'NONE',  ( -113.6268376558039108, -24.15620529776628800, 10.23563542870659582 ) ) ;
#96224=CARTESIAN_POINT ( 'NONE',  ( -82.55857454939099682, -23.73791477778912196, 11.05961554403170943 ) ) ;
#96225=CARTESIAN_POINT ( 'NONE',  ( 8.471766090126642723, -20.80389698432254519, 11.49999999999999645 ) ) ;
#96226=ORIENTED_EDGE ( 'NONE', *, *, #93926, .T. ) ;
#96228=CARTESIAN_POINT ( 'NONE',  ( 15.04091035147580335, -15.99806323810862274, 11.49999999999998934 ) ) ;
#96229=PLANE ( 'NONE',  #59215 ) ;
#96230=CARTESIAN_POINT ( 'NONE',  ( -111.6321586287164109, -23.48783264082477729, -1.443836473390087249 ) ) ;
#96231=CARTESIAN_POINT ( 'NONE',  ( -29.24636659181000198, -25.21724415148663567, 4.940287013585090925 ) ) ;
#96232=ORIENTED_EDGE ( 'NONE', *, *, #57595, .F. ) ;
#96234=CARTESIAN_POINT ( 'NONE',  ( -78.94303308397306296, -25.26642230834568537, 5.977536689587218177 ) ) ;
#96235=VERTEX_POINT ( 'NONE', #47292 ) ;
#96236=DIRECTION ( 'NONE',  ( 0.000000000000000000, -0.9999999999976377785, -2.173523156925978705E-06 ) ) ;
#96237=CARTESIAN_POINT ( 'NONE',  ( 17.04084431845542369, 11.38269047019995206, -1.500000000000002220 ) ) ;
#96238=ORIENTED_EDGE ( 'NONE', *, *, #69600, .F. ) ;
#96240=ORIENTED_EDGE ( 'NONE', *, *, #79580, .T. ) ;
#96241=CARTESIAN_POINT ( 'NONE',  ( -81.22842933447068958, -25.18098627503610132, 6.807814688516057977 ) ) ;
#96242=CARTESIAN_POINT ( 'NONE',  ( 10.19088217375349892, 20.72639945755932800, -1.500000000000002220 ) ) ;
#96243=CARTESIAN_POINT ( 'NONE',  ( -104.6305895431347466, -23.96169478059713853, 10.65365249895717525 ) ) ;
#96244=CARTESIAN_POINT ( 'NONE',  ( -16.54958403137900191, 11.88860064210666856, -1.500000000000002220 ) ) ;
#96245=VERTEX_POINT ( 'NONE', #14817 ) ;
#96246=CARTESIAN_POINT ( 'NONE',  ( -126.5228709571500616, -29.50250786944525672, 11.44777988621622633 ) ) ;
#96247=CARTESIAN_POINT ( 'NONE',  ( -51.54509106397593143, -25.21614873127006007, 3.448408489132474664 ) ) ;
#96248=CARTESIAN_POINT ( 'NONE',  ( -105.5120883362020123, -24.52300882791530512, 0.6510814631126371488 ) ) ;
#96249=CARTESIAN_POINT ( 'NONE',  ( -71.03336120160147971, -25.25855344096944677, 7.389033197858497104 ) ) ;
#96251=CARTESIAN_POINT ( 'NONE',  ( -29.22054808153496808, -25.21532083643219480, 4.231943384887517645 ) ) ;
#96252=CARTESIAN_POINT ( 'NONE',  ( -49.50841769935764347, -29.50249164770001542, 3.984438540080014413 ) ) ;
#96255=CARTESIAN_POINT ( 'NONE',  ( -16.75865769207039335, -12.26659692683164593, -1.500000000000002220 ) ) ;
#96257=CARTESIAN_POINT ( 'NONE',  ( -39.44687923781921057, -25.27828342519987359, 4.188173683033348027 ) ) ;
#96258=VERTEX_POINT ( 'NONE', #53905 ) ;
#96259=CARTESIAN_POINT ( 'NONE',  ( -86.62287095715004170, -23.48783264082478794, -1.443836473390063713 ) ) ;
#96260=CARTESIAN_POINT ( 'NONE',  ( -51.49524425620752766, -25.30370764251490812, 5.230807508121633198 ) ) ;
#96261=VERTEX_POINT ( 'NONE', #99545 ) ;
#96262=EDGE_LOOP ( 'NONE', ( #61350, #46777, #91408, #41268 ) ) ;
#96263=CARTESIAN_POINT ( 'NONE',  ( -78.62287095715007013, -23.48783264082478439, -1.443836473390065711 ) ) ;
#96264=CARTESIAN_POINT ( 'NONE',  ( -57.62287095715004881, -24.64898659630367916, 1.056161002820822592 ) ) ;
#96265=CARTESIAN_POINT ( 'NONE',  ( -71.26908920811321480, -25.31201727820361214, 5.945032220875477336 ) ) ;
#96266=CARTESIAN_POINT ( 'NONE',  ( -3.902479932019291553, -21.71820464621639246, 11.49999999999999645 ) ) ;
#96268=CARTESIAN_POINT ( 'NONE',  ( -47.62287095715004881, -24.66019654487199020, 8.947790411086133489 ) ) ;
#96269=CARTESIAN_POINT ( 'NONE',  ( 20.74359285767136640, 8.971229656761206428, -1.500000000000002220 ) ) ;
#96274=B_SPLINE_CURVE_WITH_KNOTS ( 'NONE', 3,
 ( #81364, #11846, #12341, #43310, #74249, #35693 ),
 .UNSPECIFIED., .F., .F.,
 ( 4, 2, 4 ),
 ( 0.000000000000000000, 0.001380901958385383774, 0.002761803916770767548 ),
 .UNSPECIFIED. ) ;
#96276=CARTESIAN_POINT ( 'NONE',  ( -86.58953762381671027, -23.48783264082478794, -1.443836473390063713 ) ) ;
#96277=EDGE_LOOP ( 'NONE', ( #16735, #1830, #55556, #1429 ) ) ;
#96278=CARTESIAN_POINT ( 'NONE',  ( -19.38594737788604405, 8.525550480899875438, -1.500000000000002220 ) ) ;
#96280=CARTESIAN_POINT ( 'NONE',  ( -125.6228709571500559, -24.82558206586145033, 1.605769216559438828 ) ) ;
#96281=PLANE ( 'NONE',  #19487 ) ;
#96282=CARTESIAN_POINT ( 'NONE',  ( -10.71655374829924767, -19.46388382022006525, -1.500000000000002220 ) ) ;
#96283=EDGE_CURVE ( 'NONE', #72936, #94029, #7714, .T. ) ;
#96284=CARTESIAN_POINT ( 'NONE',  ( -114.5892361776109141, -24.34968618360934656, 0.1864209137778972403 ) ) ;
#96285=EDGE_CURVE ( 'NONE', #25496, #59175, #1083, .T. ) ;
#96286=VERTEX_POINT ( 'NONE', #61525 ) ;
#96287=CARTESIAN_POINT ( 'NONE',  ( -112.5228709571501184, -23.96127896942159907, -0.6493128930933955711 ) ) ;
#96289=EDGE_CURVE ( 'NONE', #66424, #24715, #108, .T. ) ;
#96290=ADVANCED_FACE ( 'NONE', ( #37667 ), #45294, .F. ) ;
#96291=CARTESIAN_POINT ( 'NONE',  ( -41.31495979539203489, -25.15619487155882084, 3.098286890894269785 ) ) ;
#96293=CARTESIAN_POINT ( 'NONE',  ( -15.27948257512286645, 12.15582775940324822, 11.49999999999998934 ) ) ;
#96294=CARTESIAN_POINT ( 'NONE',  ( -18.57871158907727249, 10.67946855401146777, 11.49999999999998934 ) ) ;
#96296=CARTESIAN_POINT ( 'NONE',  ( -77.62287095715007013, -23.48786465467241413, 11.44779295918254469 ) ) ;
#96297=CARTESIAN_POINT ( 'NONE',  ( -77.62662168933164253, -24.51314013834315375, 0.6176544820404131775 ) ) ;
#96298=CARTESIAN_POINT ( 'NONE',  ( -16.34568771794417685, -15.85656593008108750, -1.500000000000002220 ) ) ;
#96299=VECTOR ( 'NONE', #83705, 1000.000000000000114 ) ;
#96300=CARTESIAN_POINT ( 'NONE',  ( -102.6269100961048082, -24.34968618360934656, 0.1864209137778959358 ) ) ;
#96302=CARTESIAN_POINT ( 'NONE',  ( -13.91458393394894166, 14.26456941660895339, 11.49999999999999645 ) ) ;
#96304=CARTESIAN_POINT ( 'NONE',  ( -39.57597530520470741, -24.66019654487198665, 8.947790411086131712 ) ) ;
#96305=CARTESIAN_POINT ( 'NONE',  ( -57.52287095715005449, -23.47596703998600631, 11.44779298504228926 ) ) ;
#96306=ORIENTED_EDGE ( 'NONE', *, *, #97881, .T. ) ;
#96307=CARTESIAN_POINT ( 'NONE',  ( -74.52287095715007581, -29.50250243563736774, 8.947779886222143375 ) ) ;
#96308=EDGE_CURVE ( 'NONE', #88549, #96700, #89498, .T. ) ;
#96309=CARTESIAN_POINT ( 'NONE',  ( -31.21623173926616701, -25.31516574674648368, 3.894478520810415567 ) ) ;
#96311=CARTESIAN_POINT ( 'NONE',  ( 8.489507321284875729, -19.98171680480944445, 11.49999999999998934 ) ) ;
#96312=CARTESIAN_POINT ( 'NONE',  ( -93.52287095715006160, -24.65952944569304606, 1.056160979905700570 ) ) ;
#96313=CARTESIAN_POINT ( 'NONE',  ( 15.26536572251939461, -12.21375333317339695, -1.500000000000002220 ) ) ;
#96314=CARTESIAN_POINT ( 'NONE',  ( -27.68651082257923690, -24.80976250947271211, 7.605672514646787619 ) ) ;
#96315=EDGE_CURVE ( 'NONE', #14223, #82393, #62927, .T. ) ;
#96316=ORIENTED_EDGE ( 'NONE', *, *, #9948, .T. ) ;
#96319=CARTESIAN_POINT ( 'NONE',  ( 14.97853827808193294, 13.91023239937271860, 11.49999999999999645 ) ) ;
#96320=PLANE ( 'NONE',  #97495 ) ;
#96322=EDGE_LOOP ( 'NONE', ( #71320, #52857, #37474, #79021 ) ) ;
#96323=CARTESIAN_POINT ( 'NONE',  ( -46.62287095715004881, -23.47593901973091235, -1.443836447539009749 ) ) ;
#96324=CARTESIAN_POINT ( 'NONE',  ( -39.44943695351214785, -25.18431046068020152, 4.097885212006306510 ) ) ;
#96325=DIRECTION ( 'NONE',  ( 3.773278334444167608E-23, -1.000000000000000000, 0.000000000000000000 ) ) ;
#96326=CARTESIAN_POINT ( 'NONE',  ( -88.62287095715004170, -29.50250786944525672, 11.44777988621623344 ) ) ;
#96330=CARTESIAN_POINT ( 'NONE',  ( -20.38739128398232836, 10.50225141308550292, 11.49999999999999645 ) ) ;
#96331=CARTESIAN_POINT ( 'NONE',  ( 12.23086119556625206, 19.17791753167082192, 11.49999999999998934 ) ) ;
#96333=DIRECTION ( 'NONE',  ( -3.773278334453079030E-23, 0.9999999999976377785, 2.173523156925979128E-06 ) ) ;
#96334=CARTESIAN_POINT ( 'NONE',  ( -90.62775138037345357, -24.73486907724917572, 1.287355809206966573 ) ) ;
#96337=PLANE ( 'NONE',  #90273 ) ;
#96338=EDGE_CURVE ( 'NONE', #76346, #37940, #36310, .T. ) ;
#96339=CARTESIAN_POINT ( 'NONE',  ( -6.606886629844116676, -20.84447163495035937, 11.49999999999998934 ) ) ;
#96341=CARTESIAN_POINT ( 'NONE',  ( -69.63557676323225110, -24.15620529776627734, 10.23563542870660825 ) ) ;
#96343=CARTESIAN_POINT ( 'NONE',  ( -50.38822539166535108, -25.31267346029541088, 4.736250531364077254 ) ) ;
#96344=CARTESIAN_POINT ( 'NONE',  ( -48.22287095715009286, -23.47593901973090524, -1.443836447538998424 ) ) ;
#96345=ORIENTED_EDGE ( 'NONE', *, *, #90013, .T. ) ;
#96346=CARTESIAN_POINT ( 'NONE',  ( -10.01004151551622456, -17.79114453763541093, 11.49999999999998934 ) ) ;
#96347=ORIENTED_EDGE ( 'NONE', *, *, #14850, .T. ) ;
#96348=ORIENTED_EDGE ( 'NONE', *, *, #76576, .F. ) ;
#96349=ORIENTED_EDGE ( 'NONE', *, *, #20791, .T. ) ;
#96351=B_SPLINE_CURVE_WITH_KNOTS ( 'NONE', 3,
 ( #13067, #60767, #90204, #53656, #29300, #51652, #84582, #99785, #37424, #13566 ),
 .UNSPECIFIED., .F., .F.,
 ( 4, 2, 2, 2, 4 ),
 ( 1.438708811377697253E-14, 0.0008342332072047298078, 0.001251349810799902386, 0.001459908112597480814, 0.001668466414395059242 ),
 .UNSPECIFIED. ) ;
#96352=CARTESIAN_POINT ( 'NONE',  ( -18.14924840124409045, -14.16824886576183040, -1.500000000000002220 ) ) ;
#96354=CARTESIAN_POINT ( 'NONE',  ( -7.946508460909448956, -18.53024980520100939, -1.500000000000002220 ) ) ;
#96355=VERTEX_POINT ( 'NONE', #3129 ) ;
#96356=CARTESIAN_POINT ( 'NONE',  ( -92.62287095715005592, -29.50250243563736774, 8.947779886222139822 ) ) ;
#96357=CARTESIAN_POINT ( 'NONE',  ( -49.92287095715005307, -23.47593901973090169, -1.443836447538997758 ) ) ;
#96359=CARTESIAN_POINT ( 'NONE',  ( -53.65876936014893062, -23.48786465467240347, 11.44779295918255002 ) ) ;
#96360=CARTESIAN_POINT ( 'NONE',  ( 20.50650179695670872, -5.950058665555418180, 11.49999999999999645 ) ) ;
#96361=ORIENTED_EDGE ( 'NONE', *, *, #81295, .T. ) ;
#96364=CARTESIAN_POINT ( 'NONE',  ( 18.07686251855496096, -12.98574554580779861, 11.49999999999998934 ) ) ;
#96365=CARTESIAN_POINT ( 'NONE',  ( 13.32396043830641830, 15.83023408377254704, 11.49999999999998934 ) ) ;
#96368=CARTESIAN_POINT ( 'NONE',  ( -113.5562042904834072, -24.65952944569304961, 1.056160979905704123 ) ) ;
#96369=EDGE_LOOP ( 'NONE', ( #89357, #29326, #38199, #43916 ) ) ;
#96372=CARTESIAN_POINT ( 'NONE',  ( -50.21186637932700592, -25.27517878598833789, 2.837930930803035601 ) ) ;
#96373=CARTESIAN_POINT ( 'NONE',  ( -8.674659061502078217, -19.08593140856894621, -1.500000000000002220 ) ) ;
#96374=CARTESIAN_POINT ( 'NONE',  ( 17.35060923807083810, -13.37414737355047656, 11.49999999999999645 ) ) ;
#96377=CARTESIAN_POINT ( 'NONE',  ( -6.869692127560369066, -21.44495933931894527, 11.49999999999998934 ) ) ;
#96378=CARTESIAN_POINT ( 'NONE',  ( 9.933205088616889000, -18.45388779576350302, -1.500000000000002220 ) ) ;
#96379=CARTESIAN_POINT ( 'NONE',  ( -38.52794170851076672, -24.65952944569304606, 1.056160979905694131 ) ) ;
#96382=CARTESIAN_POINT ( 'NONE',  ( -70.58953762381673869, -23.47596703998600276, 11.44779298504227505 ) ) ;
#96383=ORIENTED_EDGE ( 'NONE', *, *, #4338, .F. ) ;
#96384=VERTEX_POINT ( 'NONE', #32556 ) ;
#96386=CARTESIAN_POINT ( 'NONE',  ( -99.29755759592676156, -25.12215475168745016, 6.181036740048140743 ) ) ;
#96388=CARTESIAN_POINT ( 'NONE',  ( 14.19067371521932230, 16.14321034643037578, -1.500000000000002220 ) ) ;
#96389=EDGE_CURVE ( 'NONE', #86483, #59212, #9726, .T. ) ;
#96390=ORIENTED_EDGE ( 'NONE', *, *, #94921, .F. ) ;
#96391=CARTESIAN_POINT ( 'NONE',  ( -26.25116965330634855, -24.90568970725252385, 6.270097125102462421 ) ) ;
#96392=CARTESIAN_POINT ( 'NONE',  ( 1.225302832070333636, 21.05158420706169764, -1.500000000000002220 ) ) ;
#96394=ADVANCED_FACE ( 'NONE', ( #63530 ), #86838, .T. ) ;
#96395=CARTESIAN_POINT ( 'NONE',  ( -52.62287095715007013, -23.96127896941632685, -0.6493128931037880358 ) ) ;
#96396=CARTESIAN_POINT ( 'NONE',  ( -50.56030009453918694, -23.85049219812685095, 10.88485053497527133 ) ) ;
#96397=DIRECTION ( 'NONE',  ( 3.773278334444166432E-23, -1.000000000000000000, 0.000000000000000000 ) ) ;
#96398=CARTESIAN_POINT ( 'NONE',  ( -100.6228709571500559, -24.99132157543167310, 2.256160258750667502 ) ) ;
#96399=CARTESIAN_POINT ( 'NONE',  ( 21.95769793831392036, 2.030053023538682222, -1.500000000000002220 ) ) ;
#96400=ORIENTED_EDGE ( 'NONE', *, *, #41314, .T. ) ;
#96401=CARTESIAN_POINT ( 'NONE',  ( -65.54245111285530356, -24.52399227489126687, 9.353111116836529959 ) ) ;
#96402=ADVANCED_FACE ( 'NONE', ( #49305 ), #92314, .T. ) ;
#96405=ADVANCED_FACE ( 'NONE', ( #50795 ), #27437, .T. ) ;
#96406=CARTESIAN_POINT ( 'NONE',  ( -62.49104091010542561, -24.66019654487199730, 8.947790411086124607 ) ) ;
#96408=CARTESIAN_POINT ( 'NONE',  ( -26.12147836438646209, -24.69295662840814387, 2.461328207429541060 ) ) ;
#96411=CARTESIAN_POINT ( 'NONE',  ( 12.49974722350246736, 17.29906535522423638, 11.49999999999998934 ) ) ;
#96412=CARTESIAN_POINT ( 'NONE',  ( -104.5228709571500616, -23.96177878511309345, 10.65340807706329507 ) ) ;
#96414=CARTESIAN_POINT ( 'NONE',  ( -49.88485461511636032, -25.32724633150700200, 4.398074151685130495 ) ) ;
#96415=CARTESIAN_POINT ( 'NONE',  ( -70.58953762381673869, -24.99156044556120548, 7.747789690856344613 ) ) ;
#96416=CARTESIAN_POINT ( 'NONE',  ( -81.46835002855611663, -25.23073161514107454, 6.350709097867520470 ) ) ;
#96417=CARTESIAN_POINT ( 'NONE',  ( 22.57354875331468591, -1.174960877787051716, -1.500000000000002220 ) ) ;
#96419=CARTESIAN_POINT ( 'NONE',  ( -92.62287095715005592, -29.50250786944525672, 11.44777988621623344 ) ) ;
#96420=ORIENTED_EDGE ( 'NONE', *, *, #35464, .T. ) ;
#96421=CARTESIAN_POINT ( 'NONE',  ( -35.62287095715004170, -24.52323809116982645, 9.355190652339427260 ) ) ;
#96422=CARTESIAN_POINT ( 'NONE',  ( -42.52287095715005449, -29.50248528299804818, 1.056150453629031594 ) ) ;
#96423=CARTESIAN_POINT ( 'NONE',  ( -15.39140670439391378, -12.39996395878027791, 11.49999999999999645 ) ) ;
#96425=CARTESIAN_POINT ( 'NONE',  ( -67.49693300450357469, -24.51314013834315375, 0.6176544820404126224 ) ) ;
#96426=ORIENTED_EDGE ( 'NONE', *, *, #71839, .F. ) ;
#96428=DIRECTION ( 'NONE',  ( 3.773278334444167608E-23, -1.000000000000000000, 0.000000000000000000 ) ) ;
#96429=CARTESIAN_POINT ( 'NONE',  ( -113.6228709571500559, -24.64898659630368627, 1.056161002820831474 ) ) ;
#96430=CARTESIAN_POINT ( 'NONE',  ( -11.89702471719568244, -18.04982639819725776, -1.500000000000002220 ) ) ;
#96431=CARTESIAN_POINT ( 'NONE',  ( -86.62287095715004170, -23.48783264082478794, -1.443836473390063713 ) ) ;
#96432=CARTESIAN_POINT ( 'NONE',  ( -7.246369895950522277, -17.95243785538732340, -1.500000000000002220 ) ) ;
#96433=CARTESIAN_POINT ( 'NONE',  ( -50.55620429048338593, -23.47593901973091235, -1.443836447539009749 ) ) ;
#96435=CARTESIAN_POINT ( 'NONE',  ( 6.953341435731974940, 18.52374150113109152, 11.49999999999998934 ) ) ;
#96436=ORIENTED_EDGE ( 'NONE', *, *, #47042, .F. ) ;
#96437=CARTESIAN_POINT ( 'NONE',  ( -18.13051092187696156, -9.059970205480309957, 11.49999999999999645 ) ) ;
#96441=CARTESIAN_POINT ( 'NONE',  ( -99.83442573030144729, -25.29641444269049444, 4.527172786151116846 ) ) ;
#96445=DIRECTION ( 'NONE',  ( -1.000000000000000000, -3.773278334444166432E-23, -8.201307841325785021E-29 ) ) ;
#96446=CARTESIAN_POINT ( 'NONE',  ( 19.65109224456760728, -3.968444974485820786, 11.49999999999998934 ) ) ;
#96449=EDGE_LOOP ( 'NONE', ( #91740, #93375, #90391, #81123 ) ) ;
#96452=CARTESIAN_POINT ( 'NONE',  ( -35.52842849026595218, -24.73486907724917572, 1.287355809206972346 ) ) ;
#96455=CARTESIAN_POINT ( 'NONE',  ( -55.62287095715004170, -25.00182538069145011, 7.747789668545097541 ) ) ;
#96458=EDGE_CURVE ( 'NONE', #18521, #62579, #24062, .T. ) ;
#96459=CARTESIAN_POINT ( 'NONE',  ( -49.26249145549192576, -25.30419751004783535, 5.186272124421678953 ) ) ;
#96461=CARTESIAN_POINT ( 'NONE',  ( 8.409737122318338365, 18.51778827956368190, 11.49999999999998934 ) ) ;
#96462=VERTEX_POINT ( 'NONE', #57918 ) ;
#96463=CARTESIAN_POINT ( 'NONE',  ( 5.768980952343642166, -22.17701263744951490, 11.49999999999998934 ) ) ;
#96466=CARTESIAN_POINT ( 'NONE',  ( -37.62287095715004881, -24.50216790748098461, 0.6166512839513558220 ) ) ;
#96467=CARTESIAN_POINT ( 'NONE',  ( -50.04767967325393840, -25.12215411302513957, 7.063298327921868847 ) ) ;
#96468=CARTESIAN_POINT ( 'NONE',  ( -108.9545715455115129, -25.27705962214097113, 4.170144839539424275 ) ) ;
#96469=CARTESIAN_POINT ( 'NONE',  ( 21.17954554857512761, 0.9134790845329443520, 11.49999999999999645 ) ) ;
#96470=VECTOR ( 'NONE', #31427, 1000.000000000000114 ) ;
#96471=CARTESIAN_POINT ( 'NONE',  ( -19.05511597014879044, -11.33806725510066826, -1.500000000000002220 ) ) ;
#96473=CARTESIAN_POINT ( 'NONE',  ( 6.226698476505521995, -19.64469265145860177, 11.49999999999998934 ) ) ;
#96475=CARTESIAN_POINT ( 'NONE',  ( -50.52287095715006160, -29.50250243563736774, 8.947779886222146928 ) ) ;
#96477=CARTESIAN_POINT ( 'NONE',  ( -54.53281950657227384, -24.65952944569304606, 1.056160979905696573 ) ) ;
#96478=DIRECTION ( 'NONE',  ( -3.773278334453080206E-23, 0.9999999999976377785, 2.173523156925979975E-06 ) ) ;
#96479=ORIENTED_EDGE ( 'NONE', *, *, #14418, .F. ) ;
#96480=ORIENTED_EDGE ( 'NONE', *, *, #36637, .T. ) ;
#96483=DIRECTION ( 'NONE',  ( 0.5473879298848784991, 0.000000000000000000, -0.8368789961615403783 ) ) ;
#96486=CARTESIAN_POINT ( 'NONE',  ( -19.11632921840048738, -8.121837694355717119, -1.500000000000002220 ) ) ;
#96487=CARTESIAN_POINT ( 'NONE',  ( 21.69746526873944958, -0.4026533170205861545, 11.49999999999999645 ) ) ;
#96488=ORIENTED_EDGE ( 'NONE', *, *, #72127, .F. ) ;
#96490=CARTESIAN_POINT ( 'NONE',  ( -115.6302137719211203, -23.85016227208580730, -0.8807180028928280890 ) ) ;
#96491=CARTESIAN_POINT ( 'NONE',  ( 16.55124408090292576, 15.08944307983326638, 11.49999999999998934 ) ) ;
#96494=VERTEX_POINT ( 'NONE', #42692 ) ;
#96495=CARTESIAN_POINT ( 'NONE',  ( -31.62287095715003105, -23.96177878511307568, 10.65340807706330928 ) ) ;
#96496=CARTESIAN_POINT ( 'NONE',  ( -77.52287095715006160, -23.47596703998600631, 11.44779298504228571 ) ) ;
#96500=CARTESIAN_POINT ( 'NONE',  ( -46.54682791464076530, -24.15620529776627379, 10.23563542870660825 ) ) ;
#96501=ORIENTED_EDGE ( 'NONE', *, *, #57807, .T. ) ;
#96503=CARTESIAN_POINT ( 'NONE',  ( 21.10678091372558640, -2.468637549841573797, -1.500000000000002220 ) ) ;
#96504=ORIENTED_EDGE ( 'NONE', *, *, #29130, .F. ) ;
#96505=CARTESIAN_POINT ( 'NONE',  ( -100.9670406769712656, -25.14006151055734861, 7.002054040855493433 ) ) ;
#96506=CARTESIAN_POINT ( 'NONE',  ( -1.743439162979827595, 21.76861016152796324, 11.49999999999998934 ) ) ;
#96507=CARTESIAN_POINT ( 'NONE',  ( -128.6228709571500417, -29.50250786944525672, 11.44777988621622633 ) ) ;
#96508=CARTESIAN_POINT ( 'NONE',  ( -22.35490716430079061, -3.811827842488555440, -1.500000000000002220 ) ) ;
#96510=AXIS2_PLACEMENT_3D ( 'NONE', #37506, #99397, #53243 ) ;
#96512=CARTESIAN_POINT ( 'NONE',  ( -1.678574117887026373, -21.80011532881206548, -1.500000000000002220 ) ) ;
#96515=CARTESIAN_POINT ( 'NONE',  ( -69.62287095715005592, -23.48783264082478084, -1.443836473390067265 ) ) ;
#96518=ORIENTED_EDGE ( 'NONE', *, *, #91919, .T. ) ;
#96519=CARTESIAN_POINT ( 'NONE',  ( -30.57703644430498713, -25.30359631330190950, 3.841990343063858671 ) ) ;
#96523=CARTESIAN_POINT ( 'NONE',  ( -10.31630223030989058, -21.90544972156718018, -1.443836447538997314 ) ) ;
#96524=CARTESIAN_POINT ( 'NONE',  ( -9.505907188867841029, -19.02311915605711690, 11.49999999999998934 ) ) ;
#96525=PLANE ( 'NONE',  #67698 ) ;
#96526=EDGE_CURVE ( 'NONE', #48086, #84956, #70089, .T. ) ;
#96527=CARTESIAN_POINT ( 'NONE',  ( -26.25750150876569933, -24.75186252390866670, 3.573366613333743391 ) ) ;
#96528=CARTESIAN_POINT ( 'NONE',  ( -114.5228709571500758, -23.96127896942140367, -0.6493128930937851484 ) ) ;
#96529=CARTESIAN_POINT ( 'NONE',  ( -38.62287095715005592, -24.64965695001467694, 8.947790433994187609 ) ) ;
#96531=CARTESIAN_POINT ( 'NONE',  ( -44.62287095715004881, -23.47596703998600631, 11.44779298504227505 ) ) ;
#96532=ORIENTED_EDGE ( 'NONE', *, *, #97905, .F. ) ;
#96533=CARTESIAN_POINT ( 'NONE',  ( 17.37147561666312257, 8.948746033654231269, 11.49999999999999645 ) ) ;
#96535=DIRECTION ( 'NONE',  ( -3.773278334453079030E-23, 0.9999999999976377785, 2.173523156925979128E-06 ) ) ;
#96537=EDGE_LOOP ( 'NONE', ( #99464, #30740, #67792, #17446 ) ) ;
#96538=CARTESIAN_POINT ( 'NONE',  ( -112.6228709571500559, -29.50248528299804818, 1.056150453629043584 ) ) ;
#96539=CARTESIAN_POINT ( 'NONE',  ( -99.64934318012689118, -25.31535474791540707, 4.927356294767410105 ) ) ;
#96542=CARTESIAN_POINT ( 'NONE',  ( -16.08770303010339831, 11.32657509950784736, -1.500000000000002220 ) ) ;
#96544=AXIS2_PLACEMENT_3D ( 'NONE', #77209, #23936, #78706 ) ;
#96546=DIRECTION ( 'NONE',  ( 1.000000000000000000, 3.773278334444167608E-23, 8.201307833595939069E-29 ) ) ;
#96549=CARTESIAN_POINT ( 'NONE',  ( -74.52287095715007581, -24.65952944569304606, 1.056160979905697239 ) ) ;
#96551=CARTESIAN_POINT ( 'NONE',  ( -47.48889557811029505, -24.51314013834316086, 0.6176544820404172853 ) ) ;
#96552=CARTESIAN_POINT ( 'NONE',  ( -76.52287095715004739, -23.96127896941632329, -0.6493128931038015805 ) ) ;
#96553=CARTESIAN_POINT ( 'NONE',  ( -80.90904671513573021, -25.33009845126374771, 4.495758016894969344 ) ) ;
#96555=CARTESIAN_POINT ( 'NONE',  ( -73.52287095715007581, -24.50216790748204687, 0.6166512839542513946 ) ) ;
#96556=CARTESIAN_POINT ( 'NONE',  ( 18.73470368118781693, 6.836574088118649861, -1.500000000000002220 ) ) ;
#96557=CARTESIAN_POINT ( 'NONE',  ( -0.01697405093676656110, -22.83025757171792947, 7.289440679219588048 ) ) ;
#96558=CARTESIAN_POINT ( 'NONE',  ( 11.60740158406642664, -16.16820694497113564, -1.500000000000002220 ) ) ;
#96559=ORIENTED_EDGE ( 'NONE', *, *, #78773, .T. ) ;
#96560=CARTESIAN_POINT ( 'NONE',  ( -120.5562042904834072, -23.48783264082479150, -1.443836473390058384 ) ) ;
#96561=ADVANCED_FACE ( 'NONE', ( #27457 ), #28942, .F. ) ;
#96562=CARTESIAN_POINT ( 'NONE',  ( -93.55620429048339304, -24.66019654487199375, 8.947790411086128159 ) ) ;
#96564=CARTESIAN_POINT ( 'NONE',  ( -12.88759680649768136, 16.30154091734715749, 11.49999999999999645 ) ) ;
#96568=CARTESIAN_POINT ( 'NONE',  ( 21.14566350062385780, -8.679158401671109857, 11.49999999999999645 ) ) ;
#96569=VECTOR ( 'NONE', #11588, 1000.000000000000114 ) ;
#96570=ORIENTED_EDGE ( 'NONE', *, *, #56534, .T. ) ;
#96571=CARTESIAN_POINT ( 'NONE',  ( -64.62287095715005592, -24.65952944569304250, 1.056160979905695685 ) ) ;
#96572=CARTESIAN_POINT ( 'NONE',  ( -36.52287095715006870, -23.48786465467240347, 11.44779295918255180 ) ) ;
#96574=ORIENTED_EDGE ( 'NONE', *, *, #38443, .F. ) ;
#96575=AXIS2_PLACEMENT_3D ( 'NONE', #84173, #36501, #13653 ) ;
#96576=CARTESIAN_POINT ( 'NONE',  ( 10.87751022112437482, 17.06716278085755079, -1.500000000000002220 ) ) ;
#96578=VECTOR ( 'NONE', #33525, 1000.000000000000114 ) ;
#96581=DIRECTION ( 'NONE',  ( -3.773278334453079618E-23, 0.9999999999976377785, 2.173523156925979975E-06 ) ) ;
#96582=VERTEX_POINT ( 'NONE', #90344 ) ;
#96583=CARTESIAN_POINT ( 'NONE',  ( -79.71038897795425271, -25.31035002353226915, 4.643805851083846470 ) ) ;
#96584=CARTESIAN_POINT ( 'NONE',  ( -58.62287095715004881, -29.50248528299804818, 1.056150453629034924 ) ) ;
#96585=CARTESIAN_POINT ( 'NONE',  ( -20.04763853020464737, 0.9818187932333496404, -1.500000000000002220 ) ) ;
#96586=CARTESIAN_POINT ( 'NONE',  ( -20.81348254183067681, -2.960215062046979373, 11.49999999999999645 ) ) ;
#96587=CARTESIAN_POINT ( 'NONE',  ( -54.62287095715004170, -23.96177878511307924, 10.65340807706331105 ) ) ;
#96589=CARTESIAN_POINT ( 'NONE',  ( 18.76863814860013235, 11.56883167669432133, 11.49999999999998934 ) ) ;
#96591=CARTESIAN_POINT ( 'NONE',  ( -40.02212956655154130, -25.31589315899555359, 5.017934114441384708 ) ) ;
#96594=CARTESIAN_POINT ( 'NONE',  ( -72.65003826940696285, -23.48783264082477018, -1.443836473390095021 ) ) ;
#96595=CARTESIAN_POINT ( 'NONE',  ( -86.62287095715004170, -24.65952944569304606, 1.056160979905700348 ) ) ;
#96599=PLANE ( 'NONE',  #55121 ) ;
#96601=CARTESIAN_POINT ( 'NONE',  ( 15.21836549854886123, 13.79734045396011943, -1.500000000000002220 ) ) ;
#96604=EDGE_CURVE ( 'NONE', #76106, #88628, #51791, .T. ) ;
#96606=AXIS2_PLACEMENT_3D ( 'NONE', #32639, #11307, #41777 ) ;
#96608=CARTESIAN_POINT ( 'NONE',  ( -21.16112330106665240, 7.131417522999676351, -1.500000000000002220 ) ) ;
#96611=EDGE_LOOP ( 'NONE', ( #19316, #50479, #94041, #95361 ) ) ;
#96613=CARTESIAN_POINT ( 'NONE',  ( -51.61954071829940460, -25.29021791842099987, 4.383826557230434240 ) ) ;
#96614=CARTESIAN_POINT ( 'NONE',  ( 18.58881047053902691, 9.431966241625852732, 11.49999999999998934 ) ) ;
#96616=CARTESIAN_POINT ( 'NONE',  ( -64.62287095715005592, -29.50250243563736774, 8.947779886222145151 ) ) ;
#96620=CARTESIAN_POINT ( 'NONE',  ( 0.4554788648648982474, -21.05657754196055009, -1.500000000000002220 ) ) ;
#96623=CARTESIAN_POINT ( 'NONE',  ( -54.52287095715005449, -24.66019654487198665, 8.947790411086121054 ) ) ;
#96624=DIRECTION ( 'NONE',  ( -3.773278334453079030E-23, 0.9999999999976377785, 2.173523156925979128E-06 ) ) ;
#96625=B_SPLINE_CURVE_WITH_KNOTS ( 'NONE', 3,
 ( #13080, #90224, #99320, #75474 ),
 .UNSPECIFIED., .F., .F.,
 ( 4, 4 ),
 ( 0.2606861495984522659, 0.2696925808705678551 ),
 .UNSPECIFIED. ) ;
#96626=CARTESIAN_POINT ( 'NONE',  ( -76.53951690088622684, -24.66019654487199375, 8.947790411086119278 ) ) ;
#96628=CARTESIAN_POINT ( 'NONE',  ( 20.80172415560569021, 6.174449132348904357, -1.500000000000002220 ) ) ;
#96629=CARTESIAN_POINT ( 'NONE',  ( -80.83723253079826065, -25.12224380035756610, 7.046395587628459189 ) ) ;
#96631=CARTESIAN_POINT ( 'NONE',  ( -20.55991158545366204, 8.586518200734140294, 11.49999999999999645 ) ) ;
#96633=CARTESIAN_POINT ( 'NONE',  ( -72.62287095715002749, -24.51387760970723662, 9.387446482453421837 ) ) ;
#96634=LINE ( 'NONE', #62080, #548 ) ;
#96639=ORIENTED_EDGE ( 'NONE', *, *, #55698, .T. ) ;
#96640=VERTEX_POINT ( 'NONE', #62404 ) ;
#96643=B_SPLINE_CURVE_WITH_KNOTS ( 'NONE', 3,
 ( #97537, #29020, #58993, #52368, #82312, #20396 ),
 .UNSPECIFIED., .F., .F.,
 ( 4, 2, 4 ),
 ( 0.000000000000000000, 0.001380764517853247733, 0.002761529035706495466 ),
 .UNSPECIFIED. ) ;
#96645=CARTESIAN_POINT ( 'NONE',  ( -49.34350806497818098, -25.31059326740647109, 4.644625854372842255 ) ) ;
#96647=CARTESIAN_POINT ( 'NONE',  ( -87.52287095715007581, -24.50321055353806088, 9.387540953477520489 ) ) ;
#96648=CARTESIAN_POINT ( 'NONE',  ( -51.52287095715009002, -23.72773821059536559, 11.05748984161097326 ) ) ;
#96651=CARTESIAN_POINT ( 'NONE',  ( -130.5728709571501156, -25.00463211122487550, 1.879953029323152780 ) ) ;
#96652=CARTESIAN_POINT ( 'NONE',  ( -22.32441756149717094, -2.617931739244098388, -1.500000000000002220 ) ) ;
#96654=EDGE_CURVE ( 'NONE', #43726, #75014, #30442, .T. ) ;
#96657=DIRECTION ( 'NONE',  ( -3.773278334453079618E-23, 0.9999999999976377785, 2.173523156925979975E-06 ) ) ;
#96659=B_SPLINE_CURVE_WITH_KNOTS ( 'NONE', 3,
 ( #16540, #86567, #47516, #78441 ),
 .UNSPECIFIED., .F., .F.,
 ( 4, 4 ),
 ( 0.000000000000000000, 0.0001000000000000028644 ),
 .UNSPECIFIED. ) ;
#96660=CARTESIAN_POINT ( 'NONE',  ( -125.5228709571500332, -24.52232992886592555, 0.6492154411970870731 ) ) ;
#96662=CARTESIAN_POINT ( 'NONE',  ( -63.91870386941572946, -24.82935162629096837, 1.633150109380538950 ) ) ;
#96663=CARTESIAN_POINT ( 'NONE',  ( 16.12930680145378304, -11.13525102954884893, -1.500000000000002220 ) ) ;
#96665=VERTEX_POINT ( 'NONE', #45180 ) ;
#96666=CARTESIAN_POINT ( 'NONE',  ( -11.62584540149672385, -18.10649092712023389, -1.500000000000002220 ) ) ;
#96667=CARTESIAN_POINT ( 'NONE',  ( -129.5562042904833788, -24.64965694238575722, 8.947790433994185832 ) ) ;
#96668=CARTESIAN_POINT ( 'NONE',  ( -80.53911428444936860, -25.31572646508323743, 4.969307509984924209 ) ) ;
#96669=CARTESIAN_POINT ( 'NONE',  ( -101.2008648890725198, -25.15877266524084988, 3.052372009152386934 ) ) ;
#96671=CARTESIAN_POINT ( 'NONE',  ( 12.10309942457327992, -19.51426552955538085, -1.500000000000002220 ) ) ;
#96673=DIRECTION ( 'NONE',  ( -3.773278334453079618E-23, 0.9999999999976377785, 2.173523156925979975E-06 ) ) ;
#96674=CARTESIAN_POINT ( 'NONE',  ( -49.63955062369517890, -24.15543982623906771, -0.2315651400026657036 ) ) ;
#96675=CARTESIAN_POINT ( 'NONE',  ( 10.48293302797296356, 17.13603372422173976, 11.49999999999999645 ) ) ;
#96678=FACE_OUTER_BOUND ( 'NONE', #65983, .T. ) ;
#96680=CARTESIAN_POINT ( 'NONE',  ( -16.82575997001036328, 10.57904039763333159, 11.49999999999998934 ) ) ;
#96682=B_SPLINE_CURVE_WITH_KNOTS ( 'NONE', 3,
 ( #48931, #26080, #50426, #96587, #27086, #56048 ),
 .UNSPECIFIED., .F., .F.,
 ( 4, 2, 4 ),
 ( 1.570887131794638196E-05, 0.001396322306279763458, 0.002776935741241580609 ),
 .UNSPECIFIED. ) ;
#96683=CARTESIAN_POINT ( 'NONE',  ( -13.01991350253972080, 14.82018230214031895, -1.500000000000002220 ) ) ;
#96687=B_SPLINE_CURVE_WITH_KNOTS ( 'NONE', 3,
 ( #83231, #13712, #99447, #22317 ),
 .UNSPECIFIED., .F., .F.,
 ( 4, 4 ),
 ( 0.000000000000000000, 0.0001000000000000028644 ),
 .UNSPECIFIED. ) ;
#96688=CARTESIAN_POINT ( 'NONE',  ( -60.52287095715006160, -24.99156044556119838, 7.747789690856173195 ) ) ;
#96689=FACE_OUTER_BOUND ( 'NONE', #17479, .T. ) ;
#96690=CARTESIAN_POINT ( 'NONE',  ( -18.09956831669839872, 9.893135806712603397, 11.49999999999999645 ) ) ;
#96691=VECTOR ( 'NONE', #69575, 1000.000000000000114 ) ;
#96692=CARTESIAN_POINT ( 'NONE',  ( -33.55620429048339304, -23.47596703998600276, 11.44779298504227505 ) ) ;
#96693=CARTESIAN_POINT ( 'NONE',  ( 17.19246737676917292, 14.74310579602587090, 11.49999999999999645 ) ) ;
#96694=ADVANCED_FACE ( 'NONE', ( #83223 ), #68509, .F. ) ;
#96695=VERTEX_POINT ( 'NONE', #44678 ) ;
#96696=CARTESIAN_POINT ( 'NONE',  ( -31.24388727629348494, -24.86181185134534388, 1.747789972853592610 ) ) ;
#96697=CARTESIAN_POINT ( 'NONE',  ( -56.52287095715009002, -23.96127896941632329, -0.6493128931038024687 ) ) ;
#96698=CARTESIAN_POINT ( 'NONE',  ( -110.6228709571501128, -24.91570333823101180, 8.075032458375558164 ) ) ;
#96699=CARTESIAN_POINT ( 'NONE',  ( -128.6228709571500417, -24.65952944569305316, 1.056160979905707897 ) ) ;
#96700=VERTEX_POINT ( 'NONE', #53792 ) ;
#96701=VECTOR ( 'NONE', #59619, 1000.000000000000114 ) ;
#96702=ORIENTED_EDGE ( 'NONE', *, *, #80012, .T. ) ;
#96703=CARTESIAN_POINT ( 'NONE',  ( -98.55620429048339304, -23.47596703998600631, 11.44779298504227683 ) ) ;
#96704=CARTESIAN_POINT ( 'NONE',  ( -18.82434810282327220, -12.99595988342530362, 11.49999999999998934 ) ) ;
#96706=CARTESIAN_POINT ( 'NONE',  ( 11.83326311654409935, 18.06170320929925310, -1.500000000000002220 ) ) ;
#96707=CARTESIAN_POINT ( 'NONE',  ( -113.5177876307711529, -24.15620529776628800, 10.23563542870659582 ) ) ;
#96709=CARTESIAN_POINT ( 'NONE',  ( 3.368619518803146029, -22.26131067175759881, 11.49999999999999645 ) ) ;
#96710=ORIENTED_EDGE ( 'NONE', *, *, #33412, .T. ) ;
#96711=CARTESIAN_POINT ( 'NONE',  ( -36.55620429048340014, -23.47596703998600276, 11.44779298504227505 ) ) ;
#96712=CARTESIAN_POINT ( 'NONE',  ( 12.42595048307055983, -18.10569578304522764, 11.49999999999998934 ) ) ;
#96714=EDGE_CURVE ( 'NONE', #96746, #66619, #69003, .T. ) ;
#96715=DIRECTION ( 'NONE',  ( 1.000000000000000000, 3.773278334444167608E-23, 8.201307833595939069E-29 ) ) ;
#96716=CARTESIAN_POINT ( 'NONE',  ( -29.10172430483776651, -24.79700049711173193, 6.373704971587772050 ) ) ;
#96717=ORIENTED_EDGE ( 'NONE', *, *, #49799, .T. ) ;
#96718=CARTESIAN_POINT ( 'NONE',  ( -110.5228709571500616, -29.50247984919015209, -1.443849546365048253 ) ) ;
#96723=CARTESIAN_POINT ( 'NONE',  ( 6.429960413904108663, -19.47341730443774921, -1.500000000000002220 ) ) ;
#96725=VERTEX_POINT ( 'NONE', #60414 ) ;
#96727=EDGE_LOOP ( 'NONE', ( #51960, #35952, #95465, #3399 ) ) ;
#96728=ORIENTED_EDGE ( 'NONE', *, *, #79470, .F. ) ;
#96730=DIRECTION ( 'NONE',  ( -3.773278334453079030E-23, 0.9999999999976377785, 2.173523156925979128E-06 ) ) ;
#96731=CARTESIAN_POINT ( 'NONE',  ( -104.5196637104627087, -23.73791477778912196, 11.05961554403170410 ) ) ;
#96732=B_SPLINE_CURVE_WITH_KNOTS ( 'NONE', 3,
 ( #24019, #17418, #31633, #70206 ),
 .UNSPECIFIED., .F., .F.,
 ( 4, 4 ),
 ( 0.7292979254729236027, 0.7302986725136889623 ),
 .UNSPECIFIED. ) ;
#96733=CARTESIAN_POINT ( 'NONE',  ( -3.780122020211411193, 19.97858748211865532, -1.500000000000002220 ) ) ;
#96734=ORIENTED_EDGE ( 'NONE', *, *, #64265, .F. ) ;
#96735=CARTESIAN_POINT ( 'NONE',  ( -71.63981544056943562, -25.19546925735422960, 6.637203831572652035 ) ) ;
#96736=ADVANCED_FACE ( 'NONE', ( #38555 ), #77102, .T. ) ;
#96737=CARTESIAN_POINT ( 'NONE',  ( -29.52199316675947216, -23.40095854392973607, 11.44779303447556806 ) ) ;
#96739=EDGE_CURVE ( 'NONE', #79117, #44715, #69512, .T. ) ;
#96740=CARTESIAN_POINT ( 'NONE',  ( -105.5864570552434714, -24.83618233451450408, 1.606449574219534826 ) ) ;
#96741=CARTESIAN_POINT ( 'NONE',  ( -70.87191485471986141, -25.25855360924004245, 7.466451555984895627 ) ) ;
#96742=ORIENTED_EDGE ( 'NONE', *, *, #9109, .F. ) ;
#96743=CARTESIAN_POINT ( 'NONE',  ( -28.57654128002459260, -25.21531733429936750, 2.620673301919582254 ) ) ;
#96746=VERTEX_POINT ( 'NONE', #99930 ) ;
#96747=CARTESIAN_POINT ( 'NONE',  ( -18.43438512255917772, -9.567967903218889347, 11.49999999999998934 ) ) ;
#96748=VERTEX_POINT ( 'NONE', #83724 ) ;
#96750=ORIENTED_EDGE ( 'NONE', *, *, #21019, .F. ) ;
#96751=CARTESIAN_POINT ( 'NONE',  ( -120.5228709571501184, -23.48783264082477373, -1.443836473390081698 ) ) ;
#96755=CARTESIAN_POINT ( 'NONE',  ( -112.5895376238167245, -23.48783264082479150, -1.443836473390060160 ) ) ;
#96757=CARTESIAN_POINT ( 'NONE',  ( -52.62287095715002749, -24.51387760970724372, 9.387446482453430718 ) ) ;
#96758=CARTESIAN_POINT ( 'NONE',  ( -70.82359880940848029, -25.31201612284975155, 5.413474107398605462 ) ) ;
#96759=EDGE_CURVE ( 'NONE', #24715, #5012, #67774, .T. ) ;
#96760=CARTESIAN_POINT ( 'NONE',  ( 21.80885565983754404, 3.581153529568561478, 11.49999999999999645 ) ) ;
#96761=ORIENTED_EDGE ( 'NONE', *, *, #40753, .T. ) ;
#96762=CARTESIAN_POINT ( 'NONE',  ( -103.5510089839001466, -24.34968618360933945, 0.1864209137778842229 ) ) ;
#96763=CARTESIAN_POINT ( 'NONE',  ( -17.13258802378025791, -14.77425600068537115, 11.49999999999998934 ) ) ;
#96765=CARTESIAN_POINT ( 'NONE',  ( -115.6250716495462569, -24.73531770709096023, 8.716586749053508498 ) ) ;
#96766=ORIENTED_EDGE ( 'NONE', *, *, #35260, .T. ) ;
#96769=FACE_OUTER_BOUND ( 'NONE', #86371, .T. ) ;
#96774=CARTESIAN_POINT ( 'NONE',  ( -13.58512445790048417, 16.25115196636789250, 11.49999999999998934 ) ) ;
#96776=CARTESIAN_POINT ( 'NONE',  ( -41.52600572741248897, -25.30531391451519596, 5.104681448486787509 ) ) ;
#96777=CARTESIAN_POINT ( 'NONE',  ( 18.07686251855496096, -12.98574554580779861, -1.500000000000002220 ) ) ;
#96778=DIRECTION ( 'NONE',  ( 3.773278334444167608E-23, -1.000000000000000000, 0.000000000000000000 ) ) ;
#96782=DIRECTION ( 'NONE',  ( -3.773278334453079030E-23, 0.9999999999976377785, 2.173523156925979128E-06 ) ) ;
#96783=AXIS2_PLACEMENT_3D ( 'NONE', #9670, #95901, #65986 ) ;
#96784=EDGE_CURVE ( 'NONE', #1643, #16488, #38633, .T. ) ;
#96785=CARTESIAN_POINT ( 'NONE',  ( -36.57019847237913979, -23.48786465467240347, 11.44779295918255180 ) ) ;
#96788=CARTESIAN_POINT ( 'NONE',  ( -19.51626497420292239, -0.3564122556526727048, -1.500000000000002220 ) ) ;
#96789=CARTESIAN_POINT ( 'NONE',  ( -16.73372362409233105, 13.38858591273363174, 11.49999999999998934 ) ) ;
#96790=CARTESIAN_POINT ( 'NONE',  ( -26.25707451207771470, -24.92774811677663038, 2.297366685435383360 ) ) ;
#96792=CARTESIAN_POINT ( 'NONE',  ( -77.58809874021086728, -24.34968618360934300, 0.1864209137778811143 ) ) ;
#96793=CARTESIAN_POINT ( 'NONE',  ( 16.42120958226126604, -15.83219868413775622, -1.500000000000002220 ) ) ;
#96795=B_SPLINE_CURVE_WITH_KNOTS ( 'NONE', 3,
 ( #14549, #98279, #28786, #99284, #89690, #60748 ),
 .UNSPECIFIED., .F., .F.,
 ( 4, 2, 4 ),
 ( 0.000000000000000000, 0.001380764517853253154, 0.002761529035706506308 ),
 .UNSPECIFIED. ) ;
#96797=CARTESIAN_POINT ( 'NONE',  ( -98.50757086102233018, -24.65952944569305316, 1.056160979905702124 ) ) ;
#96799=CARTESIAN_POINT ( 'NONE',  ( 18.73470368118781693, 6.836574088118649861, 11.49999999999999645 ) ) ;
#96800=CARTESIAN_POINT ( 'NONE',  ( -78.52287095715006160, -24.64898659630367916, 1.056161002820826145 ) ) ;
#96803=B_SPLINE_CURVE_WITH_KNOTS ( 'NONE', 3,
 ( #19370, #10770, #89388, #58455 ),
 .UNSPECIFIED., .F., .F.,
 ( 4, 4 ),
 ( 2.775557561562891043E-17, 0.0001000000000000167422 ),
 .UNSPECIFIED. ) ;
#96804=CARTESIAN_POINT ( 'NONE',  ( -98.55620429048340725, -23.47593901973091235, -1.443836447539001089 ) ) ;
#96805=ORIENTED_EDGE ( 'NONE', *, *, #80131, .F. ) ;
#96806=CARTESIAN_POINT ( 'NONE',  ( -65.52287095715006160, -24.99156044556202616, 7.747789690856173195 ) ) ;
#96808=CARTESIAN_POINT ( 'NONE',  ( -17.03913561245058261, -13.47071831616118942, -1.500000000000002220 ) ) ;
#96809=CARTESIAN_POINT ( 'NONE',  ( -51.16651589987333182, -25.07168895645787643, 7.427142928140856526 ) ) ;
#96810=CARTESIAN_POINT ( 'NONE',  ( -10.28394983263804185, -16.58134856480417341, -1.500000000000002220 ) ) ;
#96813=CARTESIAN_POINT ( 'NONE',  ( -51.62287095715005592, -24.66019654487199020, 8.947790411086135265 ) ) ;
#96814=CARTESIAN_POINT ( 'NONE',  ( -19.37329759448073574, 6.469241145865432863, 11.49999999999999645 ) ) ;
#96815=LINE ( 'NONE', #28800, #73240 ) ;
#96816=CARTESIAN_POINT ( 'NONE',  ( -89.52287095715009002, -23.72747288104470087, -1.053458166803225682 ) ) ;
#96820=CARTESIAN_POINT ( 'NONE',  ( -116.5903533738907498, -24.15620529776629155, 10.23563542870659759 ) ) ;
#96821=CARTESIAN_POINT ( 'NONE',  ( -63.62287095715007723, -23.47596703998600631, 11.44779298504227683 ) ) ;
#96822=ORIENTED_EDGE ( 'NONE', *, *, #71839, .T. ) ;
#96825=CARTESIAN_POINT ( 'NONE',  ( -1.485350438481424895, -22.96994831426971828, 11.49999999999999645 ) ) ;
#96826=CARTESIAN_POINT ( 'NONE',  ( -20.37646751746074969, -10.17465561509698979, 11.49999999999998934 ) ) ;
#96827=CARTESIAN_POINT ( 'NONE',  ( -110.5493961576417519, -24.83644354573579349, 8.397322867130096569 ) ) ;
#96828=B_SPLINE_SURFACE_WITH_KNOTS ( 'NONE', 3, 3, ( 
 ( #57428, #18344, #11719, #56925 ),
 ( #42699, #18834, #27464, #49309 ),
 ( #73633, #57926, #87856, #35074 ),
 ( #66552, #88867, #20320, #80240 ),
 ( #10734, #96964, #34076, #26465 ),
 ( #58423, #35574, #97463, #27953 ),
 ( #89850, #51293, #60419, #7109 ) ),
 .UNSPECIFIED., .F., .F., .F.,
 ( 4, 3, 4 ),
 ( 4, 4 ),
 ( 0.0004766839783834262941, 0.1029713700210900945, 0.2054660560637967537 ),
 ( 0.9797432271868353748, 0.9812080034676798901 ),
 .UNSPECIFIED. ) ;
#96830=CARTESIAN_POINT ( 'NONE',  ( -120.5228709571500616, -23.47596703998600631, 11.44779298504227860 ) ) ;
#96832=CARTESIAN_POINT ( 'NONE',  ( -54.52287095715008292, -24.51283580621365132, 0.6167428607019751485 ) ) ;
#96834=CARTESIAN_POINT ( 'NONE',  ( -3.281320334969873631, 21.64054093270537393, -1.500000000000002220 ) ) ;
#96835=CARTESIAN_POINT ( 'NONE',  ( -69.59707406421517817, -23.96169478059712787, 10.65365249895718414 ) ) ;
#96839=CARTESIAN_POINT ( 'NONE',  ( -96.52287095715009002, -23.72773821059536914, 11.05748984161097681 ) ) ;
#96840=EDGE_LOOP ( 'NONE', ( #24207, #21832, #17502, #84858 ) ) ;
#96842=PRODUCT_DEFINITION_SHAPE ( 'NONE', 'NONE',  #34522 ) ;
#96843=CARTESIAN_POINT ( 'NONE',  ( 9.511415417357532931, -18.05363124325620205, 11.49999999999998934 ) ) ;
#96845=ORIENTED_EDGE ( 'NONE', *, *, #76677, .T. ) ;
#96846=ORIENTED_EDGE ( 'NONE', *, *, #51977, .T. ) ;
#96847=EDGE_LOOP ( 'NONE', ( #31598, #80784, #58319, #19707 ) ) ;
#96848=CARTESIAN_POINT ( 'NONE',  ( -1.485350438481424895, -22.96994831426971828, -1.500000000000002220 ) ) ;
#96849=DIRECTION ( 'NONE',  ( -3.773278334453079618E-23, 0.9999999999976377785, 2.173523156925979975E-06 ) ) ;
#96850=CARTESIAN_POINT ( 'NONE',  ( 12.43249465596513126, -15.92577207200969092, -1.500000000000002220 ) ) ;
#96852=CARTESIAN_POINT ( 'NONE',  ( -67.62287095715002749, -23.96177878511307568, 10.65340807706330395 ) ) ;
#96856=EDGE_CURVE ( 'NONE', #41756, #96886, #35059, .T. ) ;
#96859=CARTESIAN_POINT ( 'NONE',  ( 16.79701800048795590, -13.18750964578662455, 11.49999999999999645 ) ) ;
#96860=ORIENTED_EDGE ( 'NONE', *, *, #40279, .F. ) ;
#96862=ADVANCED_FACE ( 'NONE', ( #17724 ), #59048, .T. ) ;
#96863=ORIENTED_EDGE ( 'NONE', *, *, #55162, .F. ) ;
#96864=CARTESIAN_POINT ( 'NONE',  ( -17.34812393562427246, -13.96779696820907191, 11.49999999999998934 ) ) ;
#96865=CARTESIAN_POINT ( 'NONE',  ( 18.27903665858761073, 9.701928907310005457, 11.49999999999998934 ) ) ;
#96867=EDGE_LOOP ( 'NONE', ( #100348, #92108, #20252, #78420 ) ) ;
#96869=ORIENTED_EDGE ( 'NONE', *, *, #8120, .F. ) ;
#96871=VECTOR ( 'NONE', #51742, 1000.000000000000114 ) ;
#96872=ORIENTED_EDGE ( 'NONE', *, *, #37751, .T. ) ;
#96874=CARTESIAN_POINT ( 'NONE',  ( -18.08314111433443827, -10.61732331186343004, -1.500000000000002220 ) ) ;
#96875=EDGE_CURVE ( 'NONE', #27980, #90388, #94346, .T. ) ;
#96876=CARTESIAN_POINT ( 'NONE',  ( 21.48171311866277122, -4.276277801222842179, 11.49999999999999645 ) ) ;
#96877=CARTESIAN_POINT ( 'NONE',  ( -26.80323004365396145, -24.89279929861774221, 7.264870854583937110 ) ) ;
#96878=CARTESIAN_POINT ( 'NONE',  ( -22.36795837939145670, 2.692536522722862813, -1.500000000000002220 ) ) ;
#96879=CARTESIAN_POINT ( 'NONE',  ( 7.117523389609132778, 19.69228268689324324, -1.500000000000002220 ) ) ;
#96880=CARTESIAN_POINT ( 'NONE',  ( -110.5228709571500190, -24.91544648472626378, 1.928969306349433532 ) ) ;
#96882=CARTESIAN_POINT ( 'NONE',  ( -29.62287095715003460, -24.43778075029778307, 9.387565086202728892 ) ) ;
#96884=EDGE_CURVE ( 'NONE', #11920, #98613, #999, .T. ) ;
#96885=ORIENTED_EDGE ( 'NONE', *, *, #38762, .F. ) ;
#96886=VERTEX_POINT ( 'NONE', #40569 ) ;
#96887=ORIENTED_EDGE ( 'NONE', *, *, #45422, .T. ) ;
#96889=EDGE_LOOP ( 'NONE', ( #62941, #61205, #2824, #52302 ) ) ;
#96890=ADVANCED_FACE ( 'NONE', ( #10107 ), #69649, .T. ) ;
#96891=CARTESIAN_POINT ( 'NONE',  ( -21.47443924280258187, -0.1944818460393343829, -1.500000000000002220 ) ) ;
#96893=ORIENTED_EDGE ( 'NONE', *, *, #31078, .F. ) ;
#96894=CARTESIAN_POINT ( 'NONE',  ( 18.35617536642501690, 10.39506492455470088, 11.49999999999998934 ) ) ;
#96897=CARTESIAN_POINT ( 'NONE',  ( -43.52287095715007581, -24.66019654487199375, 8.947790411086128159 ) ) ;
#96898=CARTESIAN_POINT ( 'NONE',  ( -41.62287095715006302, -29.50248528299804818, 1.056150453629031594 ) ) ;
#96899=CARTESIAN_POINT ( 'NONE',  ( -129.5559602451679666, -23.96169478059714208, 10.65365249895717348 ) ) ;
#96900=CARTESIAN_POINT ( 'NONE',  ( -21.04927197579530329, -6.814310187297170529, -1.500000000000002220 ) ) ;
#96902=CARTESIAN_POINT ( 'NONE',  ( -81.54693475870598718, -24.35071581493543036, 9.817618358456037697 ) ) ;
#96903=CARTESIAN_POINT ( 'NONE',  ( -78.52287095715006160, -23.47593901973090169, -1.443836447538996648 ) ) ;
#96904=CARTESIAN_POINT ( 'NONE',  ( -41.77207742203299290, -25.27955894647979918, 4.730364241316486584 ) ) ;
#96905=EDGE_CURVE ( 'NONE', #40078, #52247, #93071, .T. ) ;
#96906=CARTESIAN_POINT ( 'NONE',  ( -62.58762325277358940, -24.35071581493542325, 9.817618358456032368 ) ) ;
#96908=CARTESIAN_POINT ( 'NONE',  ( -13.85510387911049079, -16.26762222697724880, 11.49999999999998934 ) ) ;
#96909=CARTESIAN_POINT ( 'NONE',  ( -26.33488822642538452, -24.89212854592702584, 6.524121854850513991 ) ) ;
#96910=CARTESIAN_POINT ( 'NONE',  ( -50.92286199449029738, -25.11539320716599377, 2.804431449967496714 ) ) ;
#96912=CARTESIAN_POINT ( 'NONE',  ( -64.59268078241893818, -24.15620529776628445, 10.23563542870660115 ) ) ;
#96914=CARTESIAN_POINT ( 'NONE',  ( -21.70561270324154179, 6.225854807558039994, -1.500000000000002220 ) ) ;
#96915=B_SPLINE_CURVE_WITH_KNOTS ( 'NONE', 3,
 ( #54728, #23248, #76035, #8033 ),
 .UNSPECIFIED., .F., .F.,
 ( 4, 4 ),
 ( 1.387778780781445521E-17, 9.999999999998898659E-05 ),
 .UNSPECIFIED. ) ;
#96916=B_SPLINE_SURFACE_WITH_KNOTS ( 'NONE', 3, 1, ( 
 ( #50762, #49773 ),
 ( #4589, #81203 ),
 ( #42165, #26918 ),
 ( #74096, #35037 ),
 ( #67482, #90310 ),
 ( #97423, #97908 ),
 ( #28401, #35539 ),
 ( #20781, #59367 ),
 ( #13171, #11193 ),
 ( #66996, #44142 ),
 ( #58872, #80704 ) ),
 .UNSPECIFIED., .F., .F., .F.,
 ( 4, 1, 1, 1, 1, 1, 1, 1, 4 ),
 ( 2, 2 ),
 ( 0.000000000000000000, 0.1182713048357273283, 0.2361775330837587172, 0.3556629329485013757, 0.4759041646706790307, 0.6001273417110856156, 0.7286081161551152263, 0.8613134756739386777, 1.000000000000000000 ),
 ( 0.000000000000000000, 1.000000000000000000 ),
 .UNSPECIFIED. ) ;
#96920=CARTESIAN_POINT ( 'NONE',  ( -79.62650269055158958, -24.51314013834315375, 0.6176544820404122893 ) ) ;
#96921=CARTESIAN_POINT ( 'NONE',  ( -13.01991350253972080, 14.82018230214031895, 11.49999999999999645 ) ) ;
#96922=CARTESIAN_POINT ( 'NONE',  ( -32.52287095715003318, -24.66019654487198665, 8.947790411086131712 ) ) ;
#96923=CARTESIAN_POINT ( 'NONE',  ( -67.64620999989506345, -23.73766607897670511, -1.055555164236457788 ) ) ;
#96925=B_SPLINE_CURVE_WITH_KNOTS ( 'NONE', 3,
 ( #32535, #33040, #88836, #41161, #72611, #71609 ),
 .UNSPECIFIED., .F., .F.,
 ( 4, 2, 4 ),
 ( 1.570887131794952276E-05, 0.001396322306279766060, 0.002776935741241582344 ),
 .UNSPECIFIED. ) ;
#96927=CARTESIAN_POINT ( 'NONE',  ( -70.52287095715006160, -24.63345952396257488, 9.038047939301513622 ) ) ;
#96928=FACE_OUTER_BOUND ( 'NONE', #64857, .T. ) ;
#96929=CARTESIAN_POINT ( 'NONE',  ( -14.23256820581467785, 16.29125061305494526, 11.49999999999998934 ) ) ;
#96930=DIRECTION ( 'NONE',  ( -1.000000000000000000, -3.773278334444166432E-23, -8.201307841325785021E-29 ) ) ;
#96932=CARTESIAN_POINT ( 'NONE',  ( 0.06232057257353295493, 19.38168652127415825, -1.500000000000002220 ) ) ;
#96934=CARTESIAN_POINT ( 'NONE',  ( -118.5895376238167245, -24.64965694238575367, 8.947790433994191162 ) ) ;
#96935=CARTESIAN_POINT ( 'NONE',  ( -19.69265041987409859, 1.759638296948408787, -1.500000000000002220 ) ) ;
#96936=ORIENTED_EDGE ( 'NONE', *, *, #60456, .F. ) ;
#96937=CARTESIAN_POINT ( 'NONE',  ( -18.19507518397214341, 8.946258903265221107, 11.49999999999999645 ) ) ;
#96938=FACE_OUTER_BOUND ( 'NONE', #30115, .T. ) ;
#96945=FACE_OUTER_BOUND ( 'NONE', #51087, .T. ) ;
#96947=CARTESIAN_POINT ( 'NONE',  ( 7.608091486120485136, 18.53616061196756704, 11.49999999999998934 ) ) ;
#96949=ORIENTED_EDGE ( 'NONE', *, *, #43351, .T. ) ;
#96952=CARTESIAN_POINT ( 'NONE',  ( -86.62287095715004170, -23.47593901973091235, -1.443836447539002865 ) ) ;
#96953=CARTESIAN_POINT ( 'NONE',  ( -79.34849387871311421, -25.27322973831870101, 5.891565427895725016 ) ) ;
#96955=CARTESIAN_POINT ( 'NONE',  ( -73.58435453540160154, -24.51314013834315375, 0.6176544820404104019 ) ) ;
#96957=CARTESIAN_POINT ( 'NONE',  ( -71.58953762381672448, -24.66019654487198665, 8.947790411086131712 ) ) ;
#96960=CARTESIAN_POINT ( 'NONE',  ( -15.70679263237263434, -12.88635299011707502, -1.500000000000002220 ) ) ;
#96961=ORIENTED_EDGE ( 'NONE', *, *, #13587, .F. ) ;
#96963=CARTESIAN_POINT ( 'NONE',  ( -22.88579126497628025, -1.409509213828211927, -1.500000000000002220 ) ) ;
#96964=CARTESIAN_POINT ( 'NONE',  ( -32.58671537039989374, -24.34968618360933590, 0.1864209137778856384 ) ) ;
#96966=ORIENTED_EDGE ( 'NONE', *, *, #36422, .F. ) ;
#96967=CARTESIAN_POINT ( 'NONE',  ( -109.5228709571500474, -23.48783264082477018, -1.443836473390083253 ) ) ;
#96969=CARTESIAN_POINT ( 'NONE',  ( -49.66108014839032592, -25.12215372425595206, 6.884432421844342009 ) ) ;
#96970=B_SPLINE_CURVE_WITH_KNOTS ( 'NONE', 3,
 ( #56879, #33023, #88311, #56379 ),
 .UNSPECIFIED., .F., .F.,
 ( 4, 4 ),
 ( 0.000000000000000000, 9.999999999998897304E-05 ),
 .UNSPECIFIED. ) ;
#96972=CARTESIAN_POINT ( 'NONE',  ( -20.37118330240554087, -5.769015352940915164, 11.49999999999999645 ) ) ;
#96973=CARTESIAN_POINT ( 'NONE',  ( 4.260453091581613450, -21.75001586557718980, -1.500000000000002220 ) ) ;
#96974=CARTESIAN_POINT ( 'NONE',  ( 6.154377932377651739, 19.64630176443789367, -1.500000000000002220 ) ) ;
#96975=ORIENTED_EDGE ( 'NONE', *, *, #6112, .T. ) ;
#96976=CARTESIAN_POINT ( 'NONE',  ( -41.53956861893506414, -24.34968618360933590, 0.1864209137778857495 ) ) ;
#96978=CARTESIAN_POINT ( 'NONE',  ( -126.6228709571500559, -29.50250786944525672, 11.44777988621622633 ) ) ;
#96979=EDGE_CURVE ( 'NONE', #79051, #43735, #84643, .T. ) ;
#96980=DIRECTION ( 'NONE',  ( 0.000000000000000000, -2.173523156925980399E-06, 0.9999999999976378895 ) ) ;
#96982=ORIENTED_EDGE ( 'NONE', *, *, #20468, .T. ) ;
#96983=ORIENTED_EDGE ( 'NONE', *, *, #45661, .F. ) ;
#96984=CARTESIAN_POINT ( 'NONE',  ( -77.52287095715007581, -24.51387760970724727, 9.387446482453412955 ) ) ;
#96986=DIRECTION ( 'NONE',  ( 0.000000000000000000, 0.9999999999976377785, 2.173523156925979975E-06 ) ) ;
#96988=CARTESIAN_POINT ( 'NONE',  ( -7.357705842588929457, 19.43699106120834230, -1.500000000000002220 ) ) ;
#96989=CARTESIAN_POINT ( 'NONE',  ( -10.76533847658563126, -18.86179312034942868, 11.49999999999999645 ) ) ;
#96990=ORIENTED_EDGE ( 'NONE', *, *, #22650, .T. ) ;
#96992=CARTESIAN_POINT ( 'NONE',  ( -96.55620429048337883, -24.65952944569304606, 1.056160979905702790 ) ) ;
#96993=CARTESIAN_POINT ( 'NONE',  ( -3.561414601982806349, 22.15502443119318343, 11.49999999999998934 ) ) ;
#96996=CARTESIAN_POINT ( 'NONE',  ( -102.5228709571501042, -23.96177878511310055, 10.65340807706329507 ) ) ;
#96997=ORIENTED_EDGE ( 'NONE', *, *, #170, .T. ) ;
#97000=ORIENTED_EDGE ( 'NONE', *, *, #94033, .F. ) ;
#97001=ORIENTED_EDGE ( 'NONE', *, *, #81178, .F. ) ;
#97002=PLANE ( 'NONE',  #39267 ) ;
#97003=ORIENTED_EDGE ( 'NONE', *, *, #11961, .F. ) ;
#97004=CARTESIAN_POINT ( 'NONE',  ( -8.160016139516647726, -19.69179572373923648, -1.500000000000002220 ) ) ;
#97005=EDGE_LOOP ( 'NONE', ( #81263, #26135, #14501, #58713 ) ) ;
#97006=CARTESIAN_POINT ( 'NONE',  ( -88.54824115366665183, -24.34968618360933945, 0.1864209137778829184 ) ) ;
#97007=CARTESIAN_POINT ( 'NONE',  ( 19.92038474643397805, 8.973206291307779026, -1.500000000000002220 ) ) ;
#97008=DIRECTION ( 'NONE',  ( 0.000000000000000000, -0.9999999999976377785, -2.173523156925979128E-06 ) ) ;
#97009=CARTESIAN_POINT ( 'NONE',  ( 19.36006514395606004, 11.85157241509795512, 11.49999999999998934 ) ) ;
#97011=CARTESIAN_POINT ( 'NONE',  ( -40.45829750704998418, -25.28892422092284420, 3.293942890672450829 ) ) ;
#97013=LINE ( 'NONE', #41747, #43307 ) ;
#97014=CARTESIAN_POINT ( 'NONE',  ( -19.93956527825925917, 9.129326121205059152, -1.500000000000002220 ) ) ;
#97015=CARTESIAN_POINT ( 'NONE',  ( -66.62287095715005592, -23.48783264082478439, -1.443836473390067487 ) ) ;
#97016=ORIENTED_EDGE ( 'NONE', *, *, #10912, .F. ) ;
#97017=CARTESIAN_POINT ( 'NONE',  ( -69.62287095715009855, -24.51283580621364422, 0.6167428607019820319 ) ) ;
#97020=ORIENTED_EDGE ( 'NONE', *, *, #76772, .F. ) ;
#97021=CARTESIAN_POINT ( 'NONE',  ( -90.62287095715004170, -23.85196035786901447, -0.8779234886475009159 ) ) ;
#97023=CARTESIAN_POINT ( 'NONE',  ( -39.56136241089613037, -25.29384247623274362, 5.536731341526268224 ) ) ;
#97024=CARTESIAN_POINT ( 'NONE',  ( -30.62052902806165733, -24.26770976782746558, 0.04347934593173557322 ) ) ;
#97025=CARTESIAN_POINT ( 'NONE',  ( 10.81949470224598997, -18.29866561848832518, -1.500000000000002220 ) ) ;
#97026=LINE ( 'NONE', #28021, #15807 ) ;
#97027=CARTESIAN_POINT ( 'NONE',  ( -27.27594984642231069, -24.75185983820420788, 2.337720939227504680 ) ) ;
#97028=EDGE_CURVE ( 'NONE', #33873, #99331, #89734, .T. ) ;
#97029=CARTESIAN_POINT ( 'NONE',  ( -80.64675904551151575, -29.50249039766296022, 3.409318347773680369 ) ) ;
#97031=B_SPLINE_CURVE_WITH_KNOTS ( 'NONE', 3,
 ( #87671, #9540, #17654, #33881 ),
 .UNSPECIFIED., .F., .F.,
 ( 4, 4 ),
 ( 0.01876752652939578034, 0.01976827357016127176 ),
 .UNSPECIFIED. ) ;
#97034=LINE ( 'NONE', #13772, #15017 ) ;
#97036=CARTESIAN_POINT ( 'NONE',  ( 2.510080532074158377, -19.39449211012750496, 11.49999999999999645 ) ) ;
#97037=CARTESIAN_POINT ( 'NONE',  ( -95.58953762381672448, -23.48783264082479150, -1.443836473390061936 ) ) ;
#97040=CARTESIAN_POINT ( 'NONE',  ( -97.52287095715007581, -23.96127896941631974, -0.6493128931037969176 ) ) ;
#97041=CARTESIAN_POINT ( 'NONE',  ( -101.6008575483875092, -25.12800596871544556, 7.076588377906173122 ) ) ;
#97042=CARTESIAN_POINT ( 'NONE',  ( -90.52287095715013265, -24.63287334234179582, 0.9662140553045340807 ) ) ;
#97043=CARTESIAN_POINT ( 'NONE',  ( -45.62287095715004881, -23.47593901973091235, -1.443836447539009749 ) ) ;
#97044=CARTESIAN_POINT ( 'NONE',  ( -13.08164486973500118, 14.69858247433046650, 11.49999999999998934 ) ) ;
#97045=ORIENTED_EDGE ( 'NONE', *, *, #1798, .F. ) ;
#97049=ORIENTED_EDGE ( 'NONE', *, *, #42705, .T. ) ;
#97052=DIRECTION ( 'NONE',  ( -3.773278334444166432E-23, 1.000000000000000000, 0.000000000000000000 ) ) ;
#97053=CARTESIAN_POINT ( 'NONE',  ( -118.6241822143420563, -24.51314013834317151, 0.6176544820404233915 ) ) ;
#97054=CARTESIAN_POINT ( 'NONE',  ( -119.5228709571500474, -23.47593901973090524, -1.443836447538996204 ) ) ;
#97059=CARTESIAN_POINT ( 'NONE',  ( -7.409219584043468920, -18.53548363135739052, -1.500000000000002220 ) ) ;
#97060=CARTESIAN_POINT ( 'NONE',  ( -0.04830472105987098502, -22.42465742606800561, 8.862518828116197511 ) ) ;
#97061=CARTESIAN_POINT ( 'NONE',  ( -5.841000908416043913, -19.03464889989004050, -1.500000000000002220 ) ) ;
#97062=ORIENTED_EDGE ( 'NONE', *, *, #59294, .F. ) ;
#97066=B_SPLINE_CURVE_WITH_KNOTS ( 'NONE', 3,
 ( #2953, #43008, #19152, #12538 ),
 .UNSPECIFIED., .F., .F.,
 ( 4, 4 ),
 ( 1.387778780781445676E-17, 0.0001000000000000028508 ),
 .UNSPECIFIED. ) ;
#97069=CARTESIAN_POINT ( 'NONE',  ( -127.4728709571500360, -25.30558663486607429, 5.000950657679038791 ) ) ;
#97073=CARTESIAN_POINT ( 'NONE',  ( -62.62287095715002039, -24.33832256526968507, 0.1851278514119872598 ) ) ;
#97074=DIRECTION ( 'NONE',  ( 0.000000000000000000, -0.9999999999976377785, -2.173523156925979975E-06 ) ) ;
#97075=ORIENTED_EDGE ( 'NONE', *, *, #78568, .T. ) ;
#97076=EDGE_CURVE ( 'NONE', #41986, #59549, #74988, .T. ) ;
#97078=( BOUNDED_SURFACE ( )  B_SPLINE_SURFACE ( 3, 1, ( 
 ( #69491, #52768 ),
 ( #91320, #7084 ),
 ( #91815, #61889 ),
 ( #22290, #38035 ) ),
 .UNSPECIFIED., .F., .F., .T. ) 
 B_SPLINE_SURFACE_WITH_KNOTS ( ( 4, 4 ),
 ( 2, 2 ),
 ( 0.000000000000000000, 1.000000000000000000 ),
 ( 0.000000000000000000, 1.000000000000000000 ),
 .UNSPECIFIED. ) 
 GEOMETRIC_REPRESENTATION_ITEM ( )  RATIONAL_B_SPLINE_SURFACE ( (
 ( 1.000000000000000000, 1.000000000000000000),
 ( 0.3333333333333332038, 0.3333333333333332038),
 ( 0.3333333333333332038, 0.3333333333333332038),
 ( 1.000000000000000000, 1.000000000000000000) ) ) 
 REPRESENTATION_ITEM ( '' )  SURFACE ( )  );
#97079=CARTESIAN_POINT ( 'NONE',  ( 13.55758662847591900, -15.04642845256218031, 11.49999999999998934 ) ) ;
#97080=CARTESIAN_POINT ( 'NONE',  ( -105.6228709571500417, -24.99156045073393173, 7.747789690856161648 ) ) ;
#97082=EDGE_CURVE ( 'NONE', #57950, #90963, #26424, .T. ) ;
#97086=CARTESIAN_POINT ( 'NONE',  ( -79.20638848209495109, -25.31561901975329576, 5.078358969147119595 ) ) ;
#97088=CARTESIAN_POINT ( 'NONE',  ( -18.95788008782500356, -6.583919088883305015, -1.500000000000002220 ) ) ;
#97089=EDGE_CURVE ( 'NONE', #14852, #69140, #14591, .T. ) ;
#97090=CARTESIAN_POINT ( 'NONE',  ( -20.98013922110768448, -1.350454208470041273, 11.49999999999999645 ) ) ;
#97092=CARTESIAN_POINT ( 'NONE',  ( -70.52205924875542564, -23.48786465467241058, 11.44779295918254824 ) ) ;
#97093=CARTESIAN_POINT ( 'NONE',  ( -21.77411086464670831, -3.637377321037103872, 11.49999999999998934 ) ) ;
#97094=ADVANCED_FACE ( 'NONE', ( #78850 ), #14088, .F. ) ;
#97095=CARTESIAN_POINT ( 'NONE',  ( -42.58953762381672448, -24.64898659630367561, 1.056161002820381833 ) ) ;
#97096=AXIS2_PLACEMENT_3D ( 'NONE', #22644, #21649, #90680 ) ;
#97097=CARTESIAN_POINT ( 'NONE',  ( -59.55620429048337883, -24.64898659630528854, 1.056161002820822814 ) ) ;
#97098=CARTESIAN_POINT ( 'NONE',  ( -50.36897396760109302, -25.27344759737253099, 3.294677657877965071 ) ) ;
#97099=ORIENTED_EDGE ( 'NONE', *, *, #17957, .T. ) ;
#97101=B_SPLINE_SURFACE_WITH_KNOTS ( 'NONE', 3, 3, ( 
 ( #67579, #5660, #89407, #68565 ),
 ( #28498, #27517, #50854, #83777 ),
 ( #14259, #52346, #81793, #28008 ),
 ( #12266, #51850, #43245, #74183 ),
 ( #35627, #58966, #91390, #20374 ),
 ( #75657, #82289, #28998, #52842 ),
 ( #68073, #45235, #12765, #76158 ) ),
 .UNSPECIFIED., .F., .F., .F.,
 ( 4, 3, 4 ),
 ( 4, 4 ),
 ( 0.7945040050992236980, 0.8970133687736494554, 0.9995227324480753239 ),
 ( 0.07951420290697416848, 0.08056363649449890807 ),
 .UNSPECIFIED. ) ;
#97102=CARTESIAN_POINT ( 'NONE',  ( -72.52287095715007581, -23.47596703998600631, 11.44779298504228748 ) ) ;
#97103=EDGE_LOOP ( 'NONE', ( #92878, #8246, #98692, #95231 ) ) ;
#97104=ORIENTED_EDGE ( 'NONE', *, *, #20468, .F. ) ;
#97105=CARTESIAN_POINT ( 'NONE',  ( -55.52287095715004028, -24.92579138211018730, 1.929029949965661128 ) ) ;
#97107=CARTESIAN_POINT ( 'NONE',  ( -76.51686571011160254, -23.73766607897670866, -1.055555164236452681 ) ) ;
#97108=EDGE_CURVE ( 'NONE', #69394, #21092, #45819, .T. ) ;
#97109=CARTESIAN_POINT ( 'NONE',  ( 16.39479758508079144, -12.47777281027006424, -1.500000000000002220 ) ) ;
#97110=CARTESIAN_POINT ( 'NONE',  ( 21.55061338234859392, -0.003183148592148328428, 11.49999999999999645 ) ) ;
#97111=VERTEX_POINT ( 'NONE', #60793 ) ;
#97113=CARTESIAN_POINT ( 'NONE',  ( -116.5228709571499905, -23.48783264083416711, -1.443836473375476270 ) ) ;
#97114=CARTESIAN_POINT ( 'NONE',  ( -60.62287095715004881, -23.47593901973091235, -1.443836447539007972 ) ) ;
#97115=CARTESIAN_POINT ( 'NONE',  ( 12.52526618502215250, 18.50471055633022388, -1.500000000000002220 ) ) ;
#97117=CARTESIAN_POINT ( 'NONE',  ( -31.55620429048338593, -23.48783264082477729, -1.443836473390074149 ) ) ;
#97118=ORIENTED_EDGE ( 'NONE', *, *, #41493, .F. ) ;
#97121=CARTESIAN_POINT ( 'NONE',  ( 7.204507412156021751, -19.57454612608841771, -1.500000000000002220 ) ) ;
#97122=ORIENTED_EDGE ( 'NONE', *, *, #58853, .F. ) ;
#97124=ORIENTED_EDGE ( 'NONE', *, *, #41302, .T. ) ;
#97125=ORIENTED_EDGE ( 'NONE', *, *, #37768, .T. ) ;
#97126=CARTESIAN_POINT ( 'NONE',  ( -51.15183413599653761, -25.29055395653329796, 4.391135634342788308 ) ) ;
#97127=CARTESIAN_POINT ( 'NONE',  ( -20.79277273739468512, 3.736189789763188607, -1.500000000000002220 ) ) ;
#97131=CARTESIAN_POINT ( 'NONE',  ( -45.52287095715007581, -25.00182538069144655, 7.747789668545101094 ) ) ;
#97133=DIRECTION ( 'NONE',  ( -3.773278334453079030E-23, 0.9999999999976377785, 2.173523156925979128E-06 ) ) ;
#97134=CARTESIAN_POINT ( 'NONE',  ( -50.30144419495010766, -25.11080889048738030, 2.835020071207171810 ) ) ;
#97135=CARTESIAN_POINT ( 'NONE',  ( -21.58526226860004371, 1.989002153404973328, -1.500000000000002220 ) ) ;
#97136=CARTESIAN_POINT ( 'NONE',  ( -63.52287095715006160, -24.66019654487199375, 8.947790411086122830 ) ) ;
#97137=CARTESIAN_POINT ( 'NONE',  ( -22.23078454666273274, -1.437644496696519170, 11.49999999999999645 ) ) ;
#97141=EDGE_CURVE ( 'NONE', #71376, #27395, #54286, .T. ) ;
#97144=VECTOR ( 'NONE', #41611, 1000.000000000000227 ) ;
#97145=CARTESIAN_POINT ( 'NONE',  ( -112.5228709571500616, -29.50250243563736774, 8.947779886222136270 ) ) ;
#97146=ORIENTED_EDGE ( 'NONE', *, *, #40427, .T. ) ;
#97148=VECTOR ( 'NONE', #29440, 1000.000000000000114 ) ;
#97149=ORIENTED_EDGE ( 'NONE', *, *, #98216, .F. ) ;
#97150=VECTOR ( 'NONE', #1115, 1000.000000000000114 ) ;
#97151=CARTESIAN_POINT ( 'NONE',  ( -100.9064891590902420, -25.14618869607998164, 7.025821505394578281 ) ) ;
#97153=CARTESIAN_POINT ( 'NONE',  ( -49.13281699349433040, -25.29228295451561337, 4.248284216210590714 ) ) ;
#97156=ADVANCED_FACE ( 'NONE', ( #84108 ), #85980, .F. ) ;
#97158=ORIENTED_EDGE ( 'NONE', *, *, #58902, .F. ) ;
#97159=CARTESIAN_POINT ( 'NONE',  ( -16.26263985875334228, -10.51264992557365829, 11.49999999999999645 ) ) ;
#97160=CARTESIAN_POINT ( 'NONE',  ( -81.52287095715006160, -23.47596703998600631, 11.44779298504228571 ) ) ;
#97161=CARTESIAN_POINT ( 'NONE',  ( 11.36419782745769069, 19.35538867594532775, -1.500000000000002220 ) ) ;
#97162=EDGE_CURVE ( 'NONE', #58574, #41451, #77242, .T. ) ;
#97163=VERTEX_POINT ( 'NONE', #24570 ) ;
#97164=CARTESIAN_POINT ( 'NONE',  ( -101.5471428905241140, -24.66019654487200086, 8.947790411086115725 ) ) ;
#97167=CARTESIAN_POINT ( 'NONE',  ( -97.23961502710135107, -25.30558673197061381, 5.002395802403323266 ) ) ;
#97168=CARTESIAN_POINT ( 'NONE',  ( 9.507684299284662188, -17.14340340408069707, 11.49999999999998934 ) ) ;
#97169=CARTESIAN_POINT ( 'NONE',  ( -119.6228709571500559, -23.47596703998600631, 11.44779298504227860 ) ) ;
#97171=CARTESIAN_POINT ( 'NONE',  ( -7.320277434469578459, 20.25297033093062282, -1.500000000000002220 ) ) ;
#97174=DIRECTION ( 'NONE',  ( 0.000000000000000000, -2.173523156925980399E-06, 0.9999999999976378895 ) ) ;
#97176=CARTESIAN_POINT ( 'NONE',  ( 20.04565040668967413, 11.27863464804978477, -1.500000000000002220 ) ) ;
#97180=CARTESIAN_POINT ( 'NONE',  ( -53.62804967469141104, -24.51314013834315730, 0.6176544820404108460 ) ) ;
#97181=CARTESIAN_POINT ( 'NONE',  ( -19.29710791919172053, 5.528754708966634901, 11.49999999999999645 ) ) ;
#97182=CARTESIAN_POINT ( 'NONE',  ( -109.5317876555421037, -25.10927444747738235, 3.055434969720114413 ) ) ;
#97183=CARTESIAN_POINT ( 'NONE',  ( -31.52287095715007581, -24.51283580621452174, 0.6167428607045826183 ) ) ;
#97187=CARTESIAN_POINT ( 'NONE',  ( -16.51628311069853083, -11.03946451426814690, 11.49999999999998934 ) ) ;
#97188=CARTESIAN_POINT ( 'NONE',  ( -113.6255566680633535, -24.34968618360934300, 0.1864209137778879699 ) ) ;
#97189=CARTESIAN_POINT ( 'NONE',  ( 17.66836560233463516, 8.693963128369697202, -1.500000000000002220 ) ) ;
#97190=CARTESIAN_POINT ( 'NONE',  ( -126.5206417414244982, -24.51419770103158058, 9.386484678747164523 ) ) ;
#97191=CARTESIAN_POINT ( 'NONE',  ( -110.5228709571500190, -24.62285846331434769, 9.038163153548369522 ) ) ;
#97193=CARTESIAN_POINT ( 'NONE',  ( 14.30100545221680441, -14.83292283143518375, 11.49999999999999645 ) ) ;
#97196=CARTESIAN_POINT ( 'NONE',  ( -7.311831771877058905, -21.45741656709679646, 11.49999999999999645 ) ) ;
#97201=EDGE_CURVE ( 'NONE', #10079, #63968, #93577, .T. ) ;
#97202=CARTESIAN_POINT ( 'NONE',  ( -101.5228709571500758, -29.50250243563736774, 8.947779886222138046 ) ) ;
#97203=CARTESIAN_POINT ( 'NONE',  ( -56.52287095715004028, -23.73934037231755667, 11.05740245334328797 ) ) ;
#97205=ORIENTED_EDGE ( 'NONE', *, *, #50882, .F. ) ;
#97208=CARTESIAN_POINT ( 'NONE',  ( 10.78062712001149492, -20.16176685268226976, 11.49999999999998934 ) ) ;
#97210=AXIS2_PLACEMENT_3D ( 'NONE', #59049, #49950, #26598 ) ;
#97211=CARTESIAN_POINT ( 'NONE',  ( 21.54666897473465070, 1.519730039111064412, -1.500000000000002220 ) ) ;
#97212=CARTESIAN_POINT ( 'NONE',  ( -94.62287095715005592, -29.50250786944525672, 11.44777988621623344 ) ) ;
#97215=CARTESIAN_POINT ( 'NONE',  ( 11.64696156460271581, 19.30390316350253244, 11.49999999999999645 ) ) ;
#97216=ORIENTED_EDGE ( 'NONE', *, *, #81869, .T. ) ;
#97218=CARTESIAN_POINT ( 'NONE',  ( -69.75794024142732042, -25.31612440964994803, 4.946031520551585459 ) ) ;
#97219=CARTESIAN_POINT ( 'NONE',  ( -9.458160343781703006, 19.84743614482962926, -1.500000000000002220 ) ) ;
#97220=EDGE_CURVE ( 'NONE', #19742, #6577, #9527, .T. ) ;
#97221=B_SPLINE_CURVE_WITH_KNOTS ( 'NONE', 3,
 ( #77281, #22988, #77776, #6290 ),
 .UNSPECIFIED., .F., .F.,
 ( 4, 4 ),
 ( 0.000000000000000000, 9.999999999997510880E-05 ),
 .UNSPECIFIED. ) ;
#97223=CARTESIAN_POINT ( 'NONE',  ( -111.6245987100719361, -24.51314013834316796, 0.6176544820404210601 ) ) ;
#97224=CARTESIAN_POINT ( 'NONE',  ( -29.24636659181000198, -24.79699738154659983, 4.940287927001176804 ) ) ;
#97225=ORIENTED_EDGE ( 'NONE', *, *, #42153, .T. ) ;
#97227=CARTESIAN_POINT ( 'NONE',  ( -35.62287095715005592, -29.50250786944525672, 11.44777988621624232 ) ) ;
#97228=VERTEX_POINT ( 'NONE', #39803 ) ;
#97229=CARTESIAN_POINT ( 'NONE',  ( -84.62287095715005592, -23.72747288104441665, -1.053458166803661111 ) ) ;
#97230=ORIENTED_EDGE ( 'NONE', *, *, #17584, .F. ) ;
#97232=ORIENTED_EDGE ( 'NONE', *, *, #82634, .F. ) ;
#97233=CARTESIAN_POINT ( 'NONE',  ( -111.2228709571500644, -23.47596703998600631, 11.44779298504227860 ) ) ;
#97237=CARTESIAN_POINT ( 'NONE',  ( -3.558151220431595707, 20.12126150705307381, -1.500000000000002220 ) ) ;
#97239=CARTESIAN_POINT ( 'NONE',  ( -71.53176178743996161, -25.15936612061949162, 6.883890870244061766 ) ) ;
#97240=CARTESIAN_POINT ( 'NONE',  ( -29.55258301704943946, -23.87856313377009698, 10.65365256123546978 ) ) ;
#97241=CARTESIAN_POINT ( 'NONE',  ( -105.5573405443120407, -23.85016227208580730, -0.8807180028928328630 ) ) ;
#97245=CARTESIAN_POINT ( 'NONE',  ( -103.6228709571500559, -24.66019654487199375, 8.947790411086124607 ) ) ;
#97246=ORIENTED_EDGE ( 'NONE', *, *, #48098, .F. ) ;
#97247=CARTESIAN_POINT ( 'NONE',  ( -5.109682455881146446, -20.12422286529520932, -1.500000000000002220 ) ) ;
#97249=CARTESIAN_POINT ( 'NONE',  ( -71.52287095715007581, -29.50248528299804818, 1.056150453629036701 ) ) ;
#97252=CARTESIAN_POINT ( 'NONE',  ( -107.6228709571500985, -24.33832256526968862, 0.1851278514119934215 ) ) ;
#97254=ORIENTED_EDGE ( 'NONE', *, *, #86035, .T. ) ;
#97256=CARTESIAN_POINT ( 'NONE',  ( -68.62287095715004170, -23.96177878511307568, 10.65340807706330217 ) ) ;
#97258=CARTESIAN_POINT ( 'NONE',  ( -43.58703515042599719, -24.35071581493542325, 9.817618358456034144 ) ) ;
#97260=CARTESIAN_POINT ( 'NONE',  ( 16.06085343747454175, -15.19291221174989204, 11.49999999999999645 ) ) ;
#97261=VERTEX_POINT ( 'NONE', #9852 ) ;
#97262=CARTESIAN_POINT ( 'NONE',  ( -63.62287095715004881, -29.50248528299804818, 1.056150453629034924 ) ) ;
#97263=CARTESIAN_POINT ( 'NONE',  ( -2.075279548881721947, -22.52154899835045043, -1.500000000000002220 ) ) ;
#97264=B_SPLINE_CURVE_WITH_KNOTS ( 'NONE', 3,
 ( #84865, #100065, #23445, #44824 ),
 .UNSPECIFIED., .F., .F.,
 ( 4, 4 ),
 ( 0.000000000000000000, 1.000000000000000000 ),
 .UNSPECIFIED. ) ;
#97265=B_SPLINE_CURVE_WITH_KNOTS ( 'NONE', 3,
 ( #14058, #92186, #52141, #83066 ),
 .UNSPECIFIED., .F., .F.,
 ( 4, 4 ),
 ( 0.06054323244033155138, 0.06954966371244711287 ),
 .UNSPECIFIED. ) ;
#97266=CARTESIAN_POINT ( 'NONE',  ( -99.46410954829916307, -25.30559305872911935, 5.025828599125619967 ) ) ;
#97269=ORIENTED_EDGE ( 'NONE', *, *, #15863, .F. ) ;
#97270=CARTESIAN_POINT ( 'NONE',  ( -75.62287095715005592, -23.48786465467241058, 11.44779295918254647 ) ) ;
#97271=AXIS2_PLACEMENT_3D ( 'NONE', #2653, #34597, #96986 ) ;
#97274=CARTESIAN_POINT ( 'NONE',  ( -57.50859435744194315, -23.96169478059713143, 10.65365249895718058 ) ) ;
#97276=CARTESIAN_POINT ( 'NONE',  ( -16.93204426113827310, 12.72334981527875186, 11.49999999999998934 ) ) ;
#97278=CARTESIAN_POINT ( 'NONE',  ( -40.93037633462841995, -25.29610591104019690, 5.483614025508329881 ) ) ;
#97279=CARTESIAN_POINT ( 'NONE',  ( 16.98343680692684643, -14.46476453587665389, -1.500000000000002220 ) ) ;
#97282=CARTESIAN_POINT ( 'NONE',  ( -65.92287095715009571, -23.47593901973090524, -1.443836447538997980 ) ) ;
#97283=CARTESIAN_POINT ( 'NONE',  ( -37.57568117332552760, -24.65952944569304606, 1.056160979905695907 ) ) ;
#97284=CARTESIAN_POINT ( 'NONE',  ( -49.62287095715004881, -23.72773821059535493, 11.05748984161097503 ) ) ;
#97287=CARTESIAN_POINT ( 'NONE',  ( -10.28394983263804185, -16.58134856480417341, -1.500000000000002220 ) ) ;
#97289=CARTESIAN_POINT ( 'NONE',  ( 19.78805588120126302, 8.271231038663975355, -1.500000000000002220 ) ) ;
#97292=CARTESIAN_POINT ( 'NONE',  ( -88.62287095715004170, -24.64965695001469115, 8.947790433994180503 ) ) ;
#97293=CARTESIAN_POINT ( 'NONE',  ( 15.15630024635751383, 17.02982414992789018, -1.500000000000002220 ) ) ;
#97294=EDGE_CURVE ( 'NONE', #37802, #65316, #96682, .T. ) ;
#97299=CARTESIAN_POINT ( 'NONE',  ( -116.5228709571500616, -29.50250786944525672, 11.44777988621622811 ) ) ;
#97300=CARTESIAN_POINT ( 'NONE',  ( -101.5562042904833930, -24.66019654487199730, 8.947790411086124607 ) ) ;
#97301=CARTESIAN_POINT ( 'NONE',  ( 14.69432462292611952, 13.40460087117274490, 11.49999999999999645 ) ) ;
#97303=CARTESIAN_POINT ( 'NONE',  ( -39.51315756755419528, -23.73791477778911130, 11.05961554403170943 ) ) ;
#97304=CARTESIAN_POINT ( 'NONE',  ( -101.6228709571500417, -23.72747288104441665, -1.053458166803661333 ) ) ;
#97307=CARTESIAN_POINT ( 'NONE',  ( -62.62287095715010565, -23.95044443724992078, 10.65354141964650125 ) ) ;
#97308=CARTESIAN_POINT ( 'NONE',  ( 3.708801897538985148, -21.39311272803122321, 11.49999999999998934 ) ) ;
#97309=EDGE_CURVE ( 'NONE', #80639, #50453, #81368, .T. ) ;
#97311=CARTESIAN_POINT ( 'NONE',  ( 11.58774116221665729, 15.72987433093905096, -1.500000000000002220 ) ) ;
#97316=FACE_OUTER_BOUND ( 'NONE', #98978, .T. ) ;
#97317=CARTESIAN_POINT ( 'NONE',  ( -7.302954156136775232, -19.11528491071161540, 11.49999999999999645 ) ) ;
#97318=CARTESIAN_POINT ( 'NONE',  ( -78.52287095715006160, -29.50250243563736774, 8.947779886222141599 ) ) ;
#97321=DIRECTION ( 'NONE',  ( -3.773278334453079030E-23, 0.9999999999976377785, 2.173523156925979128E-06 ) ) ;
#97324=EDGE_CURVE ( 'NONE', #65451, #75416, #22794, .T. ) ;
#97325=CARTESIAN_POINT ( 'NONE',  ( -67.58953762381675290, -23.47596703998600276, 11.44779298504227505 ) ) ;
#97328=CARTESIAN_POINT ( 'NONE',  ( -11.53412672884717871, -19.92380006517282709, 11.49999999999999645 ) ) ;
#97329=CARTESIAN_POINT ( 'NONE',  ( -19.53289989604362376, -11.71160353944097920, 11.49999999999998934 ) ) ;
#97330=CARTESIAN_POINT ( 'NONE',  ( -110.6324683602788923, -23.85049219812686516, 10.88485053497526955 ) ) ;
#97331=CARTESIAN_POINT ( 'NONE',  ( -122.5895376238167387, -24.64898659630368627, 1.056161002820394490 ) ) ;
#97332=CARTESIAN_POINT ( 'NONE',  ( -49.99340013130950666, -25.20303235495079619, 3.351178797549144051 ) ) ;
#97334=CARTESIAN_POINT ( 'NONE',  ( -54.55620429048340014, -23.48786465467240347, 11.44779295918255357 ) ) ;
#97336=CARTESIAN_POINT ( 'NONE',  ( -9.708950231915746798, -19.59419465507263070, 11.49999999999998934 ) ) ;
#97338=CARTESIAN_POINT ( 'NONE',  ( -59.52287095715006160, -24.64965694238407323, 8.947790433994201820 ) ) ;
#97340=B_SPLINE_CURVE_WITH_KNOTS ( 'NONE', 3,
 ( #52226, #53729, #13141, #60846 ),
 .UNSPECIFIED., .F., .F.,
 ( 4, 4 ),
 ( 0.000000000000000000, 9.999999999997510880E-05 ),
 .UNSPECIFIED. ) ;
#97341=CARTESIAN_POINT ( 'NONE',  ( -28.62287095715004881, -24.49608681932686949, 1.056161686216224860 ) ) ;
#97344=ORIENTED_EDGE ( 'NONE', *, *, #32218, .F. ) ;
#97345=CARTESIAN_POINT ( 'NONE',  ( -8.611577853089924517, -18.50786853157798006, 11.49999999999998934 ) ) ;
#97346=ORIENTED_EDGE ( 'NONE', *, *, #31323, .T. ) ;
#97347=ORIENTED_EDGE ( 'NONE', *, *, #38979, .F. ) ;
#97349=ORIENTED_EDGE ( 'NONE', *, *, #70685, .F. ) ;
#97350=CARTESIAN_POINT ( 'NONE',  ( 20.16173082093541424, 11.17373015621797627, -1.500000000000002220 ) ) ;
#97351=CARTESIAN_POINT ( 'NONE',  ( -60.52287095715008292, -23.48783264082477018, -1.443836473390092801 ) ) ;
#97353=CARTESIAN_POINT ( 'NONE',  ( -0.9278407348523283193, 20.21260682001012654, -1.500000000000002220 ) ) ;
#97354=ORIENTED_EDGE ( 'NONE', *, *, #77692, .F. ) ;
#97355=LINE ( 'NONE', #44067, #99533 ) ;
#97356=CARTESIAN_POINT ( 'NONE',  ( -34.62287095715005592, -24.64965695001467694, 8.947790433994189385 ) ) ;
#97357=EDGE_CURVE ( 'NONE', #38454, #75504, #20950, .T. ) ;
#97358=B_SPLINE_CURVE_WITH_KNOTS ( 'NONE', 3,
 ( #2555, #80170, #81669, #89281 ),
 .UNSPECIFIED., .F., .F.,
 ( 4, 4 ),
 ( 0.000000000000000000, 1.000000000000000000 ),
 .UNSPECIFIED. ) ;
#97359=VECTOR ( 'NONE', #24630, 1000.000000000000114 ) ;
#97360=CARTESIAN_POINT ( 'NONE',  ( -95.50376372625123622, -24.83618233451450408, 1.606449574219538157 ) ) ;
#97362=CARTESIAN_POINT ( 'NONE',  ( 17.72605931280000391, -11.99821887194124770, 11.49999999999999645 ) ) ;
#97364=LINE ( 'NONE', #27846, #95407 ) ;
#97365=VECTOR ( 'NONE', #85249, 1000.000000000000114 ) ;
#97367=CARTESIAN_POINT ( 'NONE',  ( -20.07822104958740539, -9.643837532803976487, -1.500000000000002220 ) ) ;
#97368=CARTESIAN_POINT ( 'NONE',  ( -17.26476610439243231, 11.37957233835482818, 11.49999999999998934 ) ) ;
#97372=CARTESIAN_POINT ( 'NONE',  ( -129.5228709571500474, -23.72747288104470798, -1.053458166803224128 ) ) ;
#97373=ORIENTED_EDGE ( 'NONE', *, *, #77633, .T. ) ;
#97374=CARTESIAN_POINT ( 'NONE',  ( -111.7814946224345789, -25.28710546256127145, 4.332404433089555695 ) ) ;
#97375=CARTESIAN_POINT ( 'NONE',  ( 17.15856466979341377, 12.00972951212132855, -1.500000000000002220 ) ) ;
#97376=CARTESIAN_POINT ( 'NONE',  ( 19.28182042344761626, 10.37885539243483812, 11.49999999999999645 ) ) ;
#97377=CARTESIAN_POINT ( 'NONE',  ( -89.50343196477413699, -24.66019654487199730, 8.947790411086115725 ) ) ;
#97378=CARTESIAN_POINT ( 'NONE',  ( -22.36795837939145670, 2.692536522722862813, 11.49999999999998934 ) ) ;
#97379=CARTESIAN_POINT ( 'NONE',  ( 10.03794737889396771, 18.37758748099471973, 11.49999999999998934 ) ) ;
#97380=FACE_OUTER_BOUND ( 'NONE', #28327, .T. ) ;
#97382=CARTESIAN_POINT ( 'NONE',  ( -119.5930762842119464, -23.48786465467241769, 11.44779295918253581 ) ) ;
#97383=CARTESIAN_POINT ( 'NONE',  ( -126.5562042904834215, -24.66019654487200086, 8.947790411086117501 ) ) ;
#97384=EDGE_CURVE ( 'NONE', #70388, #12467, #74253, .T. ) ;
#97385=ORIENTED_EDGE ( 'NONE', *, *, #21959, .T. ) ;
#97386=ORIENTED_EDGE ( 'NONE', *, *, #85761, .T. ) ;
#97387=VERTEX_POINT ( 'NONE', #4747 ) ;
#97388=CARTESIAN_POINT ( 'NONE',  ( -66.50544697010404604, -24.15543982623906771, -0.2315651400026687845 ) ) ;
#97389=B_SPLINE_CURVE_WITH_KNOTS ( 'NONE', 3,
 ( #61436, #92363, #77630, #23, #84753, #15240 ),
 .UNSPECIFIED., .F., .F.,
 ( 4, 2, 4 ),
 ( 0.000000000000000000, 0.001380764517854760195, 0.002761529035709520390 ),
 .UNSPECIFIED. ) ;
#97390=CARTESIAN_POINT ( 'NONE',  ( -2.231587876719630437, -21.34735720706076378, -1.500000000000002220 ) ) ;
#97393=CARTESIAN_POINT ( 'NONE',  ( 17.90021246794804810, -11.17811638239879279, -1.500000000000002220 ) ) ;
#97394=CARTESIAN_POINT ( 'NONE',  ( -70.75516459165498873, -25.29842503980747637, 4.197523792507152685 ) ) ;
#97398=CARTESIAN_POINT ( 'NONE',  ( -129.5558832449600857, -24.15620529776629155, 10.23563542870659759 ) ) ;
#97399=CARTESIAN_POINT ( 'NONE',  ( 16.06085343747454175, -15.19291221174989204, -1.500000000000002220 ) ) ;
#97400=CARTESIAN_POINT ( 'NONE',  ( -118.5228709571500758, -24.64898659630368627, 1.056161002820833028 ) ) ;
#97401=CARTESIAN_POINT ( 'NONE',  ( -109.3415242670784835, -25.30488224429866406, 5.187382284604649563 ) ) ;
#97403=DIRECTION ( 'NONE',  ( 0.000000000000000000, -2.173523156925980399E-06, 0.9999999999976378895 ) ) ;
#97404=CARTESIAN_POINT ( 'NONE',  ( -63.52287095715006160, -24.65952944569304606, 1.056160979905695463 ) ) ;
#97405=CARTESIAN_POINT ( 'NONE',  ( 20.50650179695670872, -5.950058665555418180, -1.500000000000002220 ) ) ;
#97409=CARTESIAN_POINT ( 'NONE',  ( -64.55379066836746915, -23.96169478059713498, 10.65365249895718058 ) ) ;
#97410=CARTESIAN_POINT ( 'NONE',  ( -53.62287095715005592, -29.50250243563736774, 8.947779886222146928 ) ) ;
#97411=B_SPLINE_CURVE_WITH_KNOTS ( 'NONE', 3,
 ( #100351, #62845, #69434, #85149, #93766, #24747, #85658, #16138 ),
 .UNSPECIFIED., .F., .F.,
 ( 4, 2, 2, 4 ),
 ( 0.000000000000000000, 0.002001098010032684085, 0.003001647015049024609, 0.004002196020065364700 ),
 .UNSPECIFIED. ) ;
#97412=CARTESIAN_POINT ( 'NONE',  ( 12.73759380600583846, -18.68238426224762350, -1.500000000000002220 ) ) ;
#97413=EDGE_CURVE ( 'NONE', #41185, #100230, #17892, .T. ) ;
#97416=CARTESIAN_POINT ( 'NONE',  ( -104.5895376238167245, -24.64965694238408034, 8.947790433994649462 ) ) ;
#97417=CARTESIAN_POINT ( 'NONE',  ( 17.61170953066113398, -8.936083093766256980, 11.49999999999999645 ) ) ;
#97418=CARTESIAN_POINT ( 'NONE',  ( -82.62287095715005592, -24.64965695001468404, 8.947790433994182280 ) ) ;
#97421=CARTESIAN_POINT ( 'NONE',  ( -89.40841769935767047, -29.50249591506787894, 5.947779886229223045 ) ) ;
#97422=CARTESIAN_POINT ( 'NONE',  ( -70.52287095715007581, -23.85229601348996198, 10.88205029486209163 ) ) ;
#97423=CARTESIAN_POINT ( 'NONE',  ( -100.8583591130402937, -25.17353330799204514, 7.041620660005706966 ) ) ;
#97425=CARTESIAN_POINT ( 'NONE',  ( -21.57582672592670292, -1.461774377805347802, 11.49999999999998934 ) ) ;
#97428=CARTESIAN_POINT ( 'NONE',  ( -40.52287095715006870, -23.47596703998600631, 11.44779298504229281 ) ) ;
#97429=EDGE_CURVE ( 'NONE', #38183, #11909, #20451, .T. ) ;
#97431=DIRECTION ( 'NONE',  ( 1.000000000000000000, 3.773278334444167608E-23, 8.201307833595939069E-29 ) ) ;
#97432=CARTESIAN_POINT ( 'NONE',  ( -15.09475962229707591, 12.77647934908296712, 11.49999999999998934 ) ) ;
#97436=CARTESIAN_POINT ( 'NONE',  ( 20.24638344296597836, 0.1212440198127159030, 11.49999999999999645 ) ) ;
#97438=CARTESIAN_POINT ( 'NONE',  ( -44.52287095715006160, -24.65952944569303895, 1.056160979905691910 ) ) ;
#97439=ORIENTED_EDGE ( 'NONE', *, *, #47622, .F. ) ;
#97440=CARTESIAN_POINT ( 'NONE',  ( -37.52287095715006160, -24.51387760970724727, 9.387446482453418284 ) ) ;
#97441=CARTESIAN_POINT ( 'NONE',  ( -28.52287095715005805, -29.50250243563660391, 8.947779535157950548 ) ) ;
#97443=CARTESIAN_POINT ( 'NONE',  ( -47.62287095715004881, -23.47593901973091235, -1.443836447539009749 ) ) ;
#97445=CARTESIAN_POINT ( 'NONE',  ( -8.782848147209532996, 18.00178819457707746, -1.500000000000002220 ) ) ;
#97447=CARTESIAN_POINT ( 'NONE',  ( -79.52287095715010423, -23.47593901973090524, -1.443836447538996870 ) ) ;
#97449=B_SPLINE_CURVE_WITH_KNOTS ( 'NONE', 3,
 ( #50991, #29632, #53493, #6788, #83412, #37745 ),
 .UNSPECIFIED., .F., .F.,
 ( 4, 2, 4 ),
 ( 1.570887131794176733E-05, 0.001396322306279759555, 0.002776935741241577573 ),
 .UNSPECIFIED. ) ;
#97450=ADVANCED_FACE ( 'NONE', ( #50764 ), #95430, .F. ) ;
#97454=CARTESIAN_POINT ( 'NONE',  ( -105.5228709571500758, -23.47593901973090524, -1.443836447538996426 ) ) ;
#97457=CARTESIAN_POINT ( 'NONE',  ( -71.62287095715005592, -24.66019654487199020, 8.947790411086131712 ) ) ;
#97459=CARTESIAN_POINT ( 'NONE',  ( -19.77321833943668850, 4.698914572609424134, -1.500000000000002220 ) ) ;
#97461=CARTESIAN_POINT ( 'NONE',  ( 6.461317529299694051, 22.01590093704556850, 11.49999999999998934 ) ) ;
#97463=CARTESIAN_POINT ( 'NONE',  ( -32.53167805950398161, -24.51314013834315375, 0.6176544820404111791 ) ) ;
#97464=ORIENTED_EDGE ( 'NONE', *, *, #70858, .T. ) ;
#97465=DIRECTION ( 'NONE',  ( 0.000000000000000000, -0.9999999999976377785, -2.173523156925979975E-06 ) ) ;
#97466=EDGE_CURVE ( 'NONE', #30992, #55957, #27600, .T. ) ;
#97467=CARTESIAN_POINT ( 'NONE',  ( -108.8968792378191921, -25.14264220134206695, 6.986250900936221697 ) ) ;
#97468=CARTESIAN_POINT ( 'NONE',  ( -38.58953762381672448, -24.66019654487199020, 8.947790411086129936 ) ) ;
#97469=CARTESIAN_POINT ( 'NONE',  ( -19.38594737788604405, 8.525550480899875438, 11.49999999999999645 ) ) ;
#97470=ORIENTED_EDGE ( 'NONE', *, *, #81840, .T. ) ;
#97471=CARTESIAN_POINT ( 'NONE',  ( -5.843409716339609261, -21.38298466452703650, 11.49999999999998934 ) ) ;
#97473=CARTESIAN_POINT ( 'NONE',  ( 18.80685554986811070, -8.408966509905500430, 11.49999999999998934 ) ) ;
#97475=ORIENTED_EDGE ( 'NONE', *, *, #77141, .F. ) ;
#97476=FACE_OUTER_BOUND ( 'NONE', #58893, .T. ) ;
#97477=B_SPLINE_CURVE_WITH_KNOTS ( 'NONE', 3,
 ( #35159, #15293, #22397, #61493, #30527, #83813 ),
 .UNSPECIFIED., .F., .F.,
 ( 4, 2, 4 ),
 ( 6.384118678620055848E-06, 0.001386860460828382791, 0.002767336802978145795 ),
 .UNSPECIFIED. ) ;
#97478=CARTESIAN_POINT ( 'NONE',  ( -70.27422298781921484, -29.50249353255212270, 4.851626040077965385 ) ) ;
#97479=ORIENTED_EDGE ( 'NONE', *, *, #76209, .F. ) ;
#97480=VERTEX_POINT ( 'NONE', #81707 ) ;
#97481=ORIENTED_EDGE ( 'NONE', *, *, #76787, .T. ) ;
#97482=CARTESIAN_POINT ( 'NONE',  ( -77.52287095715006160, -23.48786465467241058, 11.44779295918254469 ) ) ;
#97483=CARTESIAN_POINT ( 'NONE',  ( -28.58648369522600063, -24.19411652871865215, 9.817618374534072601 ) ) ;
#97484=CARTESIAN_POINT ( 'NONE',  ( -80.43221577628075636, -29.50249378334325101, 4.967010655462308577 ) ) ;
#97485=CARTESIAN_POINT ( 'NONE',  ( 5.906898857431191807, -19.90033995357616092, -1.500000000000002220 ) ) ;
#97486=CARTESIAN_POINT ( 'NONE',  ( 20.88924836996103451, 6.054424527964996194, 11.49999999999999645 ) ) ;
#97487=ORIENTED_EDGE ( 'NONE', *, *, #35331, .F. ) ;
#97488=CARTESIAN_POINT ( 'NONE',  ( -122.5228709571500758, -23.47593901973090524, -1.443836447538996204 ) ) ;
#97490=CARTESIAN_POINT ( 'NONE',  ( -19.78178409256797465, 10.57734301857266246, 11.49999999999998934 ) ) ;
#97492=CARTESIAN_POINT ( 'NONE',  ( -65.58122548746410985, -24.83618233451449697, 1.606449574219540155 ) ) ;
#97493=ORIENTED_EDGE ( 'NONE', *, *, #1253, .T. ) ;
#97494=CARTESIAN_POINT ( 'NONE',  ( -59.52287095715008292, -23.72773821059535848, 11.05748984161097681 ) ) ;
#97495=AXIS2_PLACEMENT_3D ( 'NONE', #97318, #83068, #19184 ) ;
#97496=CARTESIAN_POINT ( 'NONE',  ( -77.58953762381675290, -23.47596703998600276, 11.44779298504227683 ) ) ;
#97501=ORIENTED_EDGE ( 'NONE', *, *, #9917, .T. ) ;
#97502=CARTESIAN_POINT ( 'NONE',  ( -6.620899627221215944, -20.26055204357936290, -1.500000000000002220 ) ) ;
#97503=ORIENTED_EDGE ( 'NONE', *, *, #20672, .F. ) ;
#97505=CARTESIAN_POINT ( 'NONE',  ( 17.39636294008568740, -13.23181597624684791, 11.49999999999998934 ) ) ;
#97506=CARTESIAN_POINT ( 'NONE',  ( -45.52287095715004739, -23.48783264082477018, -1.443836473390097019 ) ) ;
#97507=CARTESIAN_POINT ( 'NONE',  ( -1.179572987637725889, 22.66035800735570049, -1.500000000000002220 ) ) ;
#97510=CARTESIAN_POINT ( 'NONE',  ( 21.92589416912191069, -1.073809401359021143, -1.500000000000002220 ) ) ;
#97514=LINE ( 'NONE', #12267, #16768 ) ;
#97516=CARTESIAN_POINT ( 'NONE',  ( -32.52287095715006160, -23.95044443724991368, 10.65354141964649948 ) ) ;
#97518=CARTESIAN_POINT ( 'NONE',  ( -10.19904569043877984, -23.73148148933709578, 3.856996771330998719 ) ) ;
#97519=CARTESIAN_POINT ( 'NONE',  ( -16.96849063341007380, -12.82450338531451450, 11.49999999999998934 ) ) ;
#97520=CARTESIAN_POINT ( 'NONE',  ( -112.6235203339132340, -24.65952944569305316, 1.056160979905707897 ) ) ;
#97521=CARTESIAN_POINT ( 'NONE',  ( -26.42246413733907673, -24.75186158583077400, 3.141773372700918721 ) ) ;
#97523=CARTESIAN_POINT ( 'NONE',  ( -68.59719488501549733, -23.96119346886880663, -0.6495511937832112448 ) ) ;
#97526=ORIENTED_EDGE ( 'NONE', *, *, #75071, .F. ) ;
#97528=CARTESIAN_POINT ( 'NONE',  ( -13.92019785312828972, -13.74635529968554515, 11.49999999999999645 ) ) ;
#97529=CARTESIAN_POINT ( 'NONE',  ( -105.5228709571500758, -23.48786465467241769, 11.44779295918253936 ) ) ;
#97530=ADVANCED_FACE ( 'NONE', ( #43154 ), #80206, .T. ) ;
#97531=CARTESIAN_POINT ( 'NONE',  ( -27.89245932500631397, -24.65620490964798250, 8.246149411531419560 ) ) ;
#97532=ORIENTED_EDGE ( 'NONE', *, *, #603, .T. ) ;
#97533=ADVANCED_FACE ( 'NONE', ( #25916 ), #94927, .F. ) ;
#97535=FACE_OUTER_BOUND ( 'NONE', #82025, .T. ) ;
#97536=EDGE_CURVE ( 'NONE', #64400, #34336, #63929, .T. ) ;
#97537=CARTESIAN_POINT ( 'NONE',  ( -31.62287095715005236, -23.47593901973091235, -1.443836447539013301 ) ) ;
#97540=CARTESIAN_POINT ( 'NONE',  ( -15.16924259816527609, 12.53091941037558854, -1.500000000000002220 ) ) ;
#97543=CARTESIAN_POINT ( 'NONE',  ( -81.52287095715006160, -29.50250786944525672, 11.44777988621623521 ) ) ;
#97547=CARTESIAN_POINT ( 'NONE',  ( -107.6228709571500701, -24.64965695001469115, 8.947790433994176951 ) ) ;
#97549=CARTESIAN_POINT ( 'NONE',  ( -47.55323112900108384, -23.96119346886880663, -0.6495511937831951466 ) ) ;
#97552=CARTESIAN_POINT ( 'NONE',  ( -69.96836528472165639, -25.31201604173465114, 5.376154465515825542 ) ) ;
#97554=CARTESIAN_POINT ( 'NONE',  ( -11.44242300287478820, -16.35863574123370512, -1.500000000000002220 ) ) ;
#97555=ADVANCED_FACE ( 'NONE', ( #3102 ), #10195, .T. ) ;
#97556=CARTESIAN_POINT ( 'NONE',  ( -32.52287095715005449, -24.50216790748203621, 0.6166512839542446223 ) ) ;
#97557=CARTESIAN_POINT ( 'NONE',  ( -0.07904045033472657800, -22.02675925722719441, 0.06506293307687280314 ) ) ;
#97558=ORIENTED_EDGE ( 'NONE', *, *, #11189, .F. ) ;
#97559=CARTESIAN_POINT ( 'NONE',  ( -63.52287095715006160, -24.64898659630367561, 1.056161002820822592 ) ) ;
#97562=EDGE_CURVE ( 'NONE', #30827, #18132, #33524, .T. ) ;
#97563=B_SPLINE_CURVE_WITH_KNOTS ( 'NONE', 3,
 ( #17124, #48093, #54210, #40475, #23732, #9516 ),
 .UNSPECIFIED., .F., .F.,
 ( 4, 2, 4 ),
 ( 6.384118678610141327E-06, 0.001386860460828372599, 0.002767336802978134953 ),
 .UNSPECIFIED. ) ;
#97566=CARTESIAN_POINT ( 'NONE',  ( -124.4728709571500360, -25.30558663486635851, 5.000950659935021747 ) ) ;
#97567=CARTESIAN_POINT ( 'NONE',  ( -81.50255920297891521, -24.51314013834316796, 0.6176544820404249458 ) ) ;
#97570=ORIENTED_EDGE ( 'NONE', *, *, #21808, .T. ) ;
#97571=FACE_OUTER_BOUND ( 'NONE', #44211, .T. ) ;
#97572=CARTESIAN_POINT ( 'NONE',  ( -127.5561563051774385, -23.73766607897670866, -1.055555164236447574 ) ) ;
#97573=ORIENTED_EDGE ( 'NONE', *, *, #27996, .T. ) ;
#97574=CARTESIAN_POINT ( 'NONE',  ( 18.19722386731275066, -8.884848157732822216, -1.500000000000002220 ) ) ;
#97575=CARTESIAN_POINT ( 'NONE',  ( -97.62287095715008434, -23.47596703998600631, 11.44779298504227860 ) ) ;
#97576=FACE_OUTER_BOUND ( 'NONE', #97982, .T. ) ;
#97578=EDGE_CURVE ( 'NONE', #83369, #59550, #69820, .T. ) ;
#97579=VERTEX_POINT ( 'NONE', #96431 ) ;
#97581=CARTESIAN_POINT ( 'NONE',  ( -105.5895376238167103, -25.00158670708909625, 2.256160236439166411 ) ) ;
#97582=CARTESIAN_POINT ( 'NONE',  ( -5.935188749463110369, 19.13178230186815298, -1.500000000000002220 ) ) ;
#97583=CARTESIAN_POINT ( 'NONE',  ( -19.40065202112720755, 8.109199488025859992, 11.49999999999999645 ) ) ;
#97584=CARTESIAN_POINT ( 'NONE',  ( -29.23548819942161003, -25.20429460498101193, 5.522040770699941703 ) ) ;
#97585=CARTESIAN_POINT ( 'NONE',  ( -70.58423071201757182, -24.73531770709095312, 8.716586749053508498 ) ) ;
#97586=CARTESIAN_POINT ( 'NONE',  ( -21.55788180805707555, 4.768121097544787190, -1.500000000000002220 ) ) ;
#97587=EDGE_CURVE ( 'NONE', #79917, #63070, #79530, .T. ) ;
#97590=CARTESIAN_POINT ( 'NONE',  ( -117.6228709571500559, -23.48786465467241769, 11.44779295918253759 ) ) ;
#97591=CARTESIAN_POINT ( 'NONE',  ( -50.20044999871004165, -25.18440104506130339, 3.305837384632741127 ) ) ;
#97592=EDGE_LOOP ( 'NONE', ( #32619, #69995, #88961, #55432 ) ) ;
#97593=FACE_OUTER_BOUND ( 'NONE', #91443, .T. ) ;
#97594=CARTESIAN_POINT ( 'NONE',  ( -31.48876216871021683, -24.34968618360933590, 0.1864209137778850556 ) ) ;
#97598=CARTESIAN_POINT ( 'NONE',  ( -89.58953762381671027, -23.48786465467241413, 11.44779295918254114 ) ) ;
#97599=PLANE ( 'NONE',  #13110 ) ;
#97600=CARTESIAN_POINT ( 'NONE',  ( -7.709890279958820258, -19.11728055126480186, -1.500000000000002220 ) ) ;
#97601=CARTESIAN_POINT ( 'NONE',  ( -21.46803524902295024, 1.580295693706654347, 11.49999999999999645 ) ) ;
#97603=CARTESIAN_POINT ( 'NONE',  ( -83.62287095715011276, -23.95044443724992789, 10.65354141964649592 ) ) ;
#97604=CARTESIAN_POINT ( 'NONE',  ( -56.58953762381671737, -24.66019654487199020, 8.947790411086133489 ) ) ;
#97605=FACE_OUTER_BOUND ( 'NONE', #76242, .T. ) ;
#97606=CARTESIAN_POINT ( 'NONE',  ( 13.15158565771796084, -18.08388448789661851, 11.49999999999998934 ) ) ;
#97609=ORIENTED_EDGE ( 'NONE', *, *, #14238, .T. ) ;
#97610=CARTESIAN_POINT ( 'NONE',  ( -94.52287095715001897, -23.73907113216990084, -1.053371485793246798 ) ) ;
#97612=AXIS2_PLACEMENT_3D ( 'NONE', #450, #56266, #55259 ) ;
#97613=CARTESIAN_POINT ( 'NONE',  ( 3.889286922045745776, 20.52237432693057073, 11.49999999999998934 ) ) ;
#97614=ORIENTED_EDGE ( 'NONE', *, *, #42697, .T. ) ;
#97615=DIRECTION ( 'NONE',  ( 0.000000000000000000, -2.173523156925980399E-06, 0.9999999999976378895 ) ) ;
#97618=CARTESIAN_POINT ( 'NONE',  ( -100.5972929639658844, -23.85049219812686161, 10.88485053497527133 ) ) ;
#97619=CARTESIAN_POINT ( 'NONE',  ( 4.565063516603933280, 20.63981631578574039, -1.500000000000002220 ) ) ;
#97623=DIRECTION ( 'NONE',  ( 0.000000000000000000, 0.9999999999976377785, 2.173523156925979128E-06 ) ) ;
#97624=CARTESIAN_POINT ( 'NONE',  ( -103.5228709571500758, -29.50248528299804818, 1.056150453629042030 ) ) ;
#97626=CARTESIAN_POINT ( 'NONE',  ( 18.41774212405765709, -11.57998961627671441, -1.500000000000002220 ) ) ;
#97627=CARTESIAN_POINT ( 'NONE',  ( -80.51244414166535535, -25.04307398257883577, 7.563174194274490780 ) ) ;
#97628=CARTESIAN_POINT ( 'NONE',  ( -20.55042600948665310, 8.738301046694649798, 11.49999999999999645 ) ) ;
#97629=ORIENTED_EDGE ( 'NONE', *, *, #88042, .F. ) ;
#97630=CARTESIAN_POINT ( 'NONE',  ( -90.52287095715006160, -29.50250786944525672, 11.44777988621623344 ) ) ;
#97635=B_SPLINE_CURVE_WITH_KNOTS ( 'NONE', 3,
 ( #32520, #2090, #41649, #56882, #64507, #86802 ),
 .UNSPECIFIED., .F., .F.,
 ( 4, 2, 4 ),
 ( 0.000000000000000000, 0.001380764517853253154, 0.002761529035706506308 ),
 .UNSPECIFIED. ) ;
#97636=AXIS2_PLACEMENT_3D ( 'NONE', #97421, #80203, #4082 ) ;
#97637=EDGE_LOOP ( 'NONE', ( #31193, #82507, #92424, #67648 ) ) ;
#97639=CARTESIAN_POINT ( 'NONE',  ( -95.52287095715006160, -24.99156044556203327, 7.747789690856173195 ) ) ;
#97642=CARTESIAN_POINT ( 'NONE',  ( -49.10841169077954049, -25.28221692862581804, 4.100616102390435280 ) ) ;
#97643=AXIS2_PLACEMENT_3D ( 'NONE', #44507, #82065, #12549 ) ;
#97645=CARTESIAN_POINT ( 'NONE',  ( -31.52287095715007581, -23.96177878511307213, 10.65340807706330750 ) ) ;
#97646=ORIENTED_EDGE ( 'NONE', *, *, #22751, .T. ) ;
#97648=CARTESIAN_POINT ( 'NONE',  ( -1.428710472040144452, 19.32843595812722626, 11.49999999999999645 ) ) ;
#97657=DIRECTION ( 'NONE',  ( -1.000000000000000000, -3.773278334444167608E-23, -8.201307833595939069E-29 ) ) ;
#97658=CARTESIAN_POINT ( 'NONE',  ( -15.96901387740391343, -11.39031854172415947, -1.500000000000002220 ) ) ;
#97659=B_SPLINE_SURFACE_WITH_KNOTS ( 'NONE', 3, 3, ( 
 ( #8137, #40084, #39074, #94862 ),
 ( #56329, #55320, #513, #61926 ),
 ( #62427, #93859, #62938, #16239 ),
 ( #15734, #46702, #86255, #16734 ),
 ( #72047, #12626, #64953, #80646 ),
 ( #34972, #26359, #33463, #81145 ),
 ( #42600, #49714, #20230, #42101 ) ),
 .UNSPECIFIED., .F., .F., .F.,
 ( 4, 3, 4 ),
 ( 4, 4 ),
 ( 0.3389040617923331777, 0.5146334493826508760, 0.6903628369729686298 ),
 ( 0.5884930944281638876, 0.6165182179194964585 ),
 .UNSPECIFIED. ) ;
#97660=EDGE_CURVE ( 'NONE', #14117, #20204, #43239, .T. ) ;
#97661=CARTESIAN_POINT ( 'NONE',  ( -46.62370088052639971, -24.65952944569304606, 1.056160979905696351 ) ) ;
#97663=CARTESIAN_POINT ( 'NONE',  ( -5.754811884962036217, -20.78327508566754389, 11.49999999999998934 ) ) ;
#97664=CARTESIAN_POINT ( 'NONE',  ( -56.62287095715005592, -24.64898659630528499, 1.056161002820822592 ) ) ;
#97665=EDGE_CURVE ( 'NONE', #53585, #62582, #82050, .T. ) ;
#97667=CARTESIAN_POINT ( 'NONE',  ( -40.57354299436993017, -23.48783264082477018, -1.443836473390102793 ) ) ;
#97668=CARTESIAN_POINT ( 'NONE',  ( -99.62727860833967952, -25.27473303363792922, 3.670122111435337953 ) ) ;
#97669=CARTESIAN_POINT ( 'NONE',  ( 10.47623847176155820, -20.49086732513842080, -1.500000000000002220 ) ) ;
#97670=AXIS2_PLACEMENT_3D ( 'NONE', #75931, #66499, #6435 ) ;
#97673=DIRECTION ( 'NONE',  ( 0.000000000000000000, -2.173523156925980399E-06, 0.9999999999976378895 ) ) ;
#97674=CARTESIAN_POINT ( 'NONE',  ( -9.895454706725905325, 17.58729670687104729, 11.49999999999999645 ) ) ;
#97675=CARTESIAN_POINT ( 'NONE',  ( -109.0059884841570153, -25.10927603167520417, 3.784296689362763644 ) ) ;
#97676=CARTESIAN_POINT ( 'NONE',  ( -32.61960262707817293, -23.48786465467240347, 11.44779295918255535 ) ) ;
#97677=DIRECTION ( 'NONE',  ( 0.000000000000000000, 2.173523156925980399E-06, -0.9999999999976378895 ) ) ;
#97680=CARTESIAN_POINT ( 'NONE',  ( -126.5895376238167529, -24.64965694238408034, 8.947790433994645909 ) ) ;
#97681=CARTESIAN_POINT ( 'NONE',  ( -12.84220538718065185, 15.17226672225704398, 11.49999999999998934 ) ) ;
#97682=VECTOR ( 'NONE', #46808, 1000.000000000000114 ) ;
#97683=CARTESIAN_POINT ( 'NONE',  ( -113.5904894942459720, -24.15543982623907837, -0.2315651400026574602 ) ) ;
#97684=CARTESIAN_POINT ( 'NONE',  ( 10.86211995951333620, 16.47970581058804740, -1.500000000000002220 ) ) ;
#97685=ADVANCED_FACE ( 'NONE', ( #28545 ), #42830, .T. ) ;
#97686=CARTESIAN_POINT ( 'NONE',  ( -126.5552517768743286, -24.35071581493544102, 9.817618358456011052 ) ) ;
#97688=CARTESIAN_POINT ( 'NONE',  ( -55.62287095715005592, -29.50247984919015209, -1.443849546365056913 ) ) ;
#97690=CARTESIAN_POINT ( 'NONE',  ( -1.706377481887368486, -20.59057665607738130, 11.49999999999999645 ) ) ;
#97693=CARTESIAN_POINT ( 'NONE',  ( -15.33504971967173702, 16.71734053393862496, 11.49999999999999645 ) ) ;
#97694=VERTEX_POINT ( 'NONE', #91435 ) ;
#97696=CARTESIAN_POINT ( 'NONE',  ( -62.52287095715006160, -23.47593901973090169, -1.443836447538997092 ) ) ;
#97698=CARTESIAN_POINT ( 'NONE',  ( -63.51556559896057053, -23.73766607897669445, -1.055555164236456900 ) ) ;
#97700=EDGE_LOOP ( 'NONE', ( #35748, #2038, #64891, #27141, #5373, #95522, #3522, #16, #31921, #30178, #66057, #66584, #45968, #23594 ) ) ;
#97702=VECTOR ( 'NONE', #54142, 1000.000000000000114 ) ;
#97704=B_SPLINE_CURVE_WITH_KNOTS ( 'NONE', 3,
 ( #18457, #19449, #64669, #64162 ),
 .UNSPECIFIED., .F., .F.,
 ( 4, 4 ),
 ( 0.000000000000000000, 9.999999999999592548E-05 ),
 .UNSPECIFIED. ) ;
#97705=CARTESIAN_POINT ( 'NONE',  ( -20.58715743568940226, -9.973749938417524774, 11.49999999999998934 ) ) ;
#97706=CARTESIAN_POINT ( 'NONE',  ( -29.65134019565081047, -23.88568904270062276, -0.6495508823503304274 ) ) ;
#97707=CARTESIAN_POINT ( 'NONE',  ( -16.67190562677319932, -13.68652177170558204, -1.500000000000002220 ) ) ;
#97708=CARTESIAN_POINT ( 'NONE',  ( -113.5585651354342502, -23.48786465467241058, 11.44779295918254292 ) ) ;
#97709=FACE_OUTER_BOUND ( 'NONE', #98281, .T. ) ;
#97711=CARTESIAN_POINT ( 'NONE',  ( 6.936750662203477802, 21.44973376661030429, 11.49999999999999645 ) ) ;
#97713=CARTESIAN_POINT ( 'NONE',  ( -28.24471377493544111, -24.85223738551369266, 2.395901059869563809 ) ) ;
#97714=CARTESIAN_POINT ( 'NONE',  ( 12.93620265873104991, 17.78788284566447331, -1.500000000000002220 ) ) ;
#97715=CARTESIAN_POINT ( 'NONE',  ( -111.5868598658171891, -24.65952944569305316, 1.056160979905705455 ) ) ;
#97716=CARTESIAN_POINT ( 'NONE',  ( -70.52287095715007581, -25.00182538069145366, 7.747789668545101094 ) ) ;
#97718=VERTEX_POINT ( 'NONE', #21917 ) ;
#97719=CARTESIAN_POINT ( 'NONE',  ( -98.52287095715006160, -29.50250243563736774, 8.947779886222138046 ) ) ;
#97721=DIRECTION ( 'NONE',  ( 0.000000000000000000, -2.173523156925979552E-06, 0.9999999999976378895 ) ) ;
#97722=ORIENTED_EDGE ( 'NONE', *, *, #74300, .T. ) ;
#97723=CARTESIAN_POINT ( 'NONE',  ( -84.62287095715007013, -23.94994826722515668, -0.6494450866351710872 ) ) ;
#97724=ORIENTED_EDGE ( 'NONE', *, *, #17492, .F. ) ;
#97727=CARTESIAN_POINT ( 'NONE',  ( -49.73963891290676287, -25.31032741935931440, 5.370288135609136759 ) ) ;
#97728=LINE ( 'NONE', #50560, #11294 ) ;
#97729=CARTESIAN_POINT ( 'NONE',  ( -57.65691505428798536, -23.48783264082477018, -1.443836473390095243 ) ) ;
#97730=CARTESIAN_POINT ( 'NONE',  ( 5.749347661499963458, 19.61174949527739386, -1.500000000000002220 ) ) ;
#97731=EDGE_CURVE ( 'NONE', #85265, #44470, #36040, .T. ) ;
#97732=ORIENTED_EDGE ( 'NONE', *, *, #16817, .T. ) ;
#97735=CARTESIAN_POINT ( 'NONE',  ( -105.5995553614588403, -23.48783264082477018, -1.443836473390094355 ) ) ;
#97736=FACE_OUTER_BOUND ( 'NONE', #73648, .T. ) ;
#97737=ORIENTED_EDGE ( 'NONE', *, *, #91797, .F. ) ;
#97738=CARTESIAN_POINT ( 'NONE',  ( -122.9228709571500389, -23.47593901973090524, -1.443836447538996426 ) ) ;
#97739=CARTESIAN_POINT ( 'NONE',  ( -27.99827674658315502, -25.26248072559767266, 8.232206008816641329 ) ) ;
#97740=EDGE_LOOP ( 'NONE', ( #86384, #53003, #8024, #100166 ) ) ;
#97741=CARTESIAN_POINT ( 'NONE',  ( -2.100290975465340271, -20.70549805216813510, 11.49999999999998934 ) ) ;
#97742=ORIENTED_EDGE ( 'NONE', *, *, #51787, .T. ) ;
#97744=CARTESIAN_POINT ( 'NONE',  ( -39.78242746767242721, -25.30509143442804998, 4.885129823892348178 ) ) ;
#97745=ORIENTED_EDGE ( 'NONE', *, *, #35696, .F. ) ;
#97746=B_SPLINE_SURFACE_WITH_KNOTS ( 'NONE', 3, 1, ( 
 ( #88079, #18553 ),
 ( #80959, #71856 ),
 ( #64261, #56639 ),
 ( #87570, #10949 ),
 ( #49022, #41914 ),
 ( #3357, #83945 ),
 ( #44401, #27676 ),
 ( #12436, #97182 ),
 ( #20054, #89570 ),
 ( #52009, #67244 ),
 ( #67745, #51513 ),
 ( #22027, #58625 ),
 ( #51016, #13927 ),
 ( #45400, #53015 ),
 ( #12928, #97675 ),
 ( #5823, #81952 ),
 ( #5324, #43897 ),
 ( #60633, #35787 ),
 ( #82939, #66258 ) ),
 .UNSPECIFIED., .F., .F., .F.,
 ( 4, 1, 1, 1, 1, 1, 1, 1, 1, 1, 1, 1, 1, 1, 1, 1, 4 ),
 ( 2, 2 ),
 ( 0.000000000000000000, 0.06947546024967000966, 0.1365167976177991127, 0.2007888236092598422, 0.2638296728558247040, 0.3257350229654227269, 0.3872906922152893339, 0.4495092187626021918, 0.5129678195454410172, 0.5762752154930611548, 0.6375801002639256421, 0.6979026059171035135, 0.7571720884269868002, 0.8165985284886555506, 0.8766531708928191335, 0.9372896424102402646, 1.000000000000000000 ),
 ( 0.000000000000000000, 1.000000000000000000 ),
 .UNSPECIFIED. ) ;
#97748=CARTESIAN_POINT ( 'NONE',  ( -52.52287095715006870, -23.48786465467241058, 11.44779295918255002 ) ) ;
#97750=ORIENTED_EDGE ( 'NONE', *, *, #74125, .T. ) ;
#97751=CARTESIAN_POINT ( 'NONE',  ( -79.52287095715006160, -24.65952944569304961, 1.056160979905698794 ) ) ;
#97752=CARTESIAN_POINT ( 'NONE',  ( -121.2228709571500218, -23.47593901973090524, -1.443836447538996204 ) ) ;
#97753=CARTESIAN_POINT ( 'NONE',  ( -80.52287095715006160, -25.00158670708909625, 2.256160236439166411 ) ) ;
#97754=CARTESIAN_POINT ( 'NONE',  ( -71.15736797201716968, -25.24515128636431527, 5.711157537062583778 ) ) ;
#97755=CARTESIAN_POINT ( 'NONE',  ( -16.84257673422482426, -14.26466048179180568, 11.49999999999999645 ) ) ;
#97756=VERTEX_POINT ( 'NONE', #86340 ) ;
#97757=CARTESIAN_POINT ( 'NONE',  ( -108.5134097286098722, -24.51314013834316086, 0.6176544820404235026 ) ) ;
#97758=AXIS2_PLACEMENT_3D ( 'NONE', #52074, #28230, #83001 ) ;
#97759=CARTESIAN_POINT ( 'NONE',  ( 18.79633983808273712, -12.56333175589740847, 11.49999999999998934 ) ) ;
#97760=CARTESIAN_POINT ( 'NONE',  ( -46.52287095715006160, -23.73934037231757088, 11.05740245334329153 ) ) ;
#97761=ORIENTED_EDGE ( 'NONE', *, *, #89344, .T. ) ;
#97762=VECTOR ( 'NONE', #36909, 1000.000000000000114 ) ;
#97765=B_SPLINE_CURVE_WITH_KNOTS ( 'NONE', 3,
 ( #34320, #50052, #72389, #95216 ),
 .UNSPECIFIED., .F., .F.,
 ( 4, 4 ),
 ( 0.000000000000000000, 9.999999999998897304E-05 ),
 .UNSPECIFIED. ) ;
#97769=CARTESIAN_POINT ( 'NONE',  ( -21.75032768068154354, -4.810781854073628239, -1.500000000000002220 ) ) ;
#97771=ORIENTED_EDGE ( 'NONE', *, *, #22783, .F. ) ;
#97777=CARTESIAN_POINT ( 'NONE',  ( -14.81708852449743929, -12.69844354874750181, 11.49999999999998934 ) ) ;
#97778=ADVANCED_FACE ( 'NONE', ( #46778 ), #82539, .T. ) ;
#97779=CARTESIAN_POINT ( 'NONE',  ( 0.5228555243449846124, 21.43159495547403282, -1.500000000000002220 ) ) ;
#97781=ADVANCED_FACE ( 'NONE', ( #69620 ), #70113, .F. ) ;
#97782=DIRECTION ( 'NONE',  ( -1.000000000000000000, -3.773278334444167608E-23, -8.201307833595939069E-29 ) ) ;
#97783=DIRECTION ( 'NONE',  ( -1.000000000000000000, -3.773278334444166432E-23, -8.201307841325785021E-29 ) ) ;
#97784=CARTESIAN_POINT ( 'NONE',  ( -17.61067154241388977, 14.45706175128816184, -1.500000000000002220 ) ) ;
#97788=LINE ( 'NONE', #72977, #578 ) ;
#97789=CARTESIAN_POINT ( 'NONE',  ( 17.55240489776628721, -9.587225365216566431, 11.49999999999999645 ) ) ;
#97790=CARTESIAN_POINT ( 'NONE',  ( -104.6266640182791008, -24.34968618360934300, 0.1864209137778872205 ) ) ;
#97792=CARTESIAN_POINT ( 'NONE',  ( -39.52202212734117381, -23.48786465467240347, 11.44779295918255002 ) ) ;
#97793=CARTESIAN_POINT ( 'NONE',  ( -48.62834717164137288, -24.51314013834315375, 0.6176544820404137326 ) ) ;
#97794=ORIENTED_EDGE ( 'NONE', *, *, #16200, .F. ) ;
#97795=EDGE_CURVE ( 'NONE', #28755, #33442, #86832, .T. ) ;
#97798=CARTESIAN_POINT ( 'NONE',  ( 17.51545567653809954, -12.82042131148251229, -1.500000000000002220 ) ) ;
#97800=CARTESIAN_POINT ( 'NONE',  ( -8.292788067677484776, 17.68049324621676632, -1.500000000000002220 ) ) ;
#97801=DIRECTION ( 'NONE',  ( -3.773278334444166432E-23, 1.000000000000000000, 0.000000000000000000 ) ) ;
#97802=ORIENTED_EDGE ( 'NONE', *, *, #25519, .T. ) ;
#97804=FACE_OUTER_BOUND ( 'NONE', #9611, .T. ) ;
#97805=CARTESIAN_POINT ( 'NONE',  ( -110.6228709571500985, -24.83602698348161297, 1.605859176311268399 ) ) ;
#97806=CARTESIAN_POINT ( 'NONE',  ( 1.124825640313904973, 20.40429917142216354, 11.49999999999999645 ) ) ;
#97808=CARTESIAN_POINT ( 'NONE',  ( -93.58953762381671027, -23.48783264082478794, -1.443836473390063713 ) ) ;
#97809=EDGE_LOOP ( 'NONE', ( #79504, #75081, #28363, #36876 ) ) ;
#97810=CARTESIAN_POINT ( 'NONE',  ( -51.58953762381673158, -23.47593901973091235, -1.443836447539009749 ) ) ;
#97811=DIRECTION ( 'NONE',  ( -3.773278334453079030E-23, 0.9999999999976377785, 2.173523156925979128E-06 ) ) ;
#97812=CARTESIAN_POINT ( 'NONE',  ( -116.5567474348173675, -23.73791477778912551, 11.05961554403170055 ) ) ;
#97816=ORIENTED_EDGE ( 'NONE', *, *, #47305, .T. ) ;
#97819=CARTESIAN_POINT ( 'NONE',  ( -19.18584950847915493, -12.73052202388904952, 11.49999999999999645 ) ) ;
#97820=CARTESIAN_POINT ( 'NONE',  ( -17.51746294255814718, -14.55262482891283504, 11.49999999999998934 ) ) ;
#97821=CARTESIAN_POINT ( 'NONE',  ( -110.5222005053990557, -23.48786465467241413, 11.44779295918253581 ) ) ;
#97823=CARTESIAN_POINT ( 'NONE',  ( -120.5228709571500616, -24.99156044556120904, 7.747789690856173195 ) ) ;
#97824=CARTESIAN_POINT ( 'NONE',  ( -50.58953762381673158, -25.00158670708909625, 2.256160236439164635 ) ) ;
#97825=CARTESIAN_POINT ( 'NONE',  ( -110.5103941636743485, -25.00158670708910336, 2.256160236439219258 ) ) ;
#97826=CARTESIAN_POINT ( 'NONE',  ( -9.857428550561325054, -19.57614489166009264, -1.500000000000002220 ) ) ;
#97829=CARTESIAN_POINT ( 'NONE',  ( -103.6228709571500559, -24.66019654487199375, 8.947790411086124607 ) ) ;
#97830=CARTESIAN_POINT ( 'NONE',  ( -71.60138352291718888, -25.29053162850427583, 5.617232799301285162 ) ) ;
#97831=CARTESIAN_POINT ( 'NONE',  ( -28.62287095715004881, -29.50247984919086264, -1.443849221408822103 ) ) ;
#97833=CARTESIAN_POINT ( 'NONE',  ( 17.38039551199336685, -10.77953091123627694, 11.49999999999998934 ) ) ;
#97835=ORIENTED_EDGE ( 'NONE', *, *, #7723, .F. ) ;
#97837=ORIENTED_EDGE ( 'NONE', *, *, #44409, .F. ) ;
#97838=CARTESIAN_POINT ( 'NONE',  ( 1.550618966079767347, 22.99078241098900932, -1.500000000000002220 ) ) ;
#97839=CARTESIAN_POINT ( 'NONE',  ( -61.58322304524284618, -24.51314013834316441, 0.6176544820404165081 ) ) ;
#97840=CARTESIAN_POINT ( 'NONE',  ( -9.806399893892750796, 17.69452640759178408, -1.500000000000002220 ) ) ;
#97842=PLANE ( 'NONE',  #60685 ) ;
#97843=CARTESIAN_POINT ( 'NONE',  ( -127.5228709571500616, -24.64965694238408034, 8.947790433994189385 ) ) ;
#97846=CARTESIAN_POINT ( 'NONE',  ( -19.74196057798672399, -8.316236533413031040, 11.49999999999999645 ) ) ;
#97847=VERTEX_POINT ( 'NONE', #40674 ) ;
#97848=CARTESIAN_POINT ( 'NONE',  ( -77.58953762381672448, -23.48783264082478794, -1.443836473390065933 ) ) ;
#97850=CARTESIAN_POINT ( 'NONE',  ( 0.6114060112162268412, -22.25658958135186793, -1.500000000000002220 ) ) ;
#97851=CARTESIAN_POINT ( 'NONE',  ( 19.89799572200132971, -5.707369160466581270, 11.49999999999998934 ) ) ;
#97854=CARTESIAN_POINT ( 'NONE',  ( -28.55248484695741595, -23.80080791946256014, -0.6495505116914124244 ) ) ;
#97855=ORIENTED_EDGE ( 'NONE', *, *, #47073, .T. ) ;
#97856=DIRECTION ( 'NONE',  ( 0.000000000000000000, 2.173523156925980399E-06, -0.9999999999976378895 ) ) ;
#97858=CARTESIAN_POINT ( 'NONE',  ( -3.950822543831816080, -20.53616823614468956, -1.500000000000002220 ) ) ;
#97859=CARTESIAN_POINT ( 'NONE',  ( -3.478157889954244464, -21.63767827151469447, 11.49999999999999645 ) ) ;
#97860=CARTESIAN_POINT ( 'NONE',  ( -91.58953762381672448, -24.65952944569304606, 1.056160979905697239 ) ) ;
#97861=CARTESIAN_POINT ( 'NONE',  ( -12.86601690267178100, 18.50254183665605012, 11.49999999999998934 ) ) ;
#97862=EDGE_CURVE ( 'NONE', #2525, #79654, #95346, .T. ) ;
#97863=CARTESIAN_POINT ( 'NONE',  ( 11.42219733811748306, 17.55150860717643724, -1.500000000000002220 ) ) ;
#97864=DIRECTION ( 'NONE',  ( 0.000000000000000000, -2.173523156925980399E-06, 0.9999999999976378895 ) ) ;
#97866=FACE_OUTER_BOUND ( 'NONE', #78491, .T. ) ;
#97867=EDGE_LOOP ( 'NONE', ( #37630, #16890, #72333, #34255 ) ) ;
#97868=EDGE_LOOP ( 'NONE', ( #62247, #66005, #21371, #37577 ) ) ;
#97870=CARTESIAN_POINT ( 'NONE',  ( -66.59743583313027671, -23.96119346886880308, -0.6495511937832151306 ) ) ;
#97871=CARTESIAN_POINT ( 'NONE',  ( -15.31780299886000485, -15.04297462106122474, -1.500000000000002220 ) ) ;
#97872=CARTESIAN_POINT ( 'NONE',  ( -86.62287095715005592, -24.66019654487199375, 8.947790411086124607 ) ) ;
#97874=CARTESIAN_POINT ( 'NONE',  ( -20.97943885474387216, 2.004451313549292735, 11.49999999999998934 ) ) ;
#97875=CARTESIAN_POINT ( 'NONE',  ( -99.52885836007774856, -25.26978538596253188, 3.946409558071873214 ) ) ;
#97876=LINE ( 'NONE', #59333, #25242 ) ;
#97880=CARTESIAN_POINT ( 'NONE',  ( -8.904070064990065703, -20.24664451029508783, -1.500000000000002220 ) ) ;
#97881=EDGE_CURVE ( 'NONE', #75111, #34031, #27451, .T. ) ;
#97882=CARTESIAN_POINT ( 'NONE',  ( -116.5525168704854195, -24.51314013834316086, 0.6176544820404277214 ) ) ;
#97883=EDGE_CURVE ( 'NONE', #29958, #85000, #3359, .T. ) ;
#97885=CARTESIAN_POINT ( 'NONE',  ( -109.1632612664256357, -25.30553889313048543, 4.924919525099058504 ) ) ;
#97886=CARTESIAN_POINT ( 'NONE',  ( -99.52287095715011844, -24.33927499327856481, 9.819080762295815390 ) ) ;
#97887=CARTESIAN_POINT ( 'NONE',  ( -58.58953762381671027, -23.47593901973091235, -1.443836447539007972 ) ) ;
#97889=CARTESIAN_POINT ( 'NONE',  ( 1.664315604108443925, 19.36118569274438528, -1.500000000000002220 ) ) ;
#97890=CARTESIAN_POINT ( 'NONE',  ( 19.59546714036918758, 8.467717511154198462, -1.500000000000002220 ) ) ;
#97891=FACE_OUTER_BOUND ( 'NONE', #60673, .T. ) ;
#97892=CARTESIAN_POINT ( 'NONE',  ( -51.94981768477178008, -25.25978491487771649, 3.590542621692356384 ) ) ;
#97893=EDGE_CURVE ( 'NONE', #13741, #44036, #51677, .T. ) ;
#97894=DIRECTION ( 'NONE',  ( -3.773278334444166432E-23, 1.000000000000000000, 0.000000000000000000 ) ) ;
#97895=CARTESIAN_POINT ( 'NONE',  ( -70.74026866089612042, -25.30511070033976395, 4.894904393956083233 ) ) ;
#97896=CARTESIAN_POINT ( 'NONE',  ( 17.73637878876437668, -14.10177982315242318, -1.500000000000002220 ) ) ;
#97900=CARTESIAN_POINT ( 'NONE',  ( -79.59586967038401895, -23.96119346886880308, -0.6495511937832122440 ) ) ;
#97901=CARTESIAN_POINT ( 'NONE',  ( 5.037983044326730386, -19.10262670698400100, 11.49999999999999645 ) ) ;
#97902=CARTESIAN_POINT ( 'NONE',  ( -50.52287095715006160, -29.50247984919015209, -1.443849546365058689 ) ) ;
#97903=PLANE ( 'NONE',  #82973 ) ;
#97905=EDGE_CURVE ( 'NONE', #77370, #13904, #16623, .T. ) ;
#97906=CARTESIAN_POINT ( 'NONE',  ( -59.52287095715006160, -24.64898659630528854, 1.056161002820822592 ) ) ;
#97907=DIRECTION ( 'NONE',  ( -1.000000000000000000, -3.773278334444167608E-23, -8.201307833595939069E-29 ) ) ;
#97908=CARTESIAN_POINT ( 'NONE',  ( -100.8583591130402937, -25.12268552722101944, 7.041620770524536610 ) ) ;
#97909=CARTESIAN_POINT ( 'NONE',  ( -16.54959454218438708, 13.92943311328891554, -1.500000000000002220 ) ) ;
#97910=CARTESIAN_POINT ( 'NONE',  ( -49.19632817692706084, -25.10935285274896245, 3.560434298826884447 ) ) ;
#97911=CARTESIAN_POINT ( 'NONE',  ( -15.38109395195050233, 11.78095549196778258, -1.500000000000002220 ) ) ;
#97913=CARTESIAN_POINT ( 'NONE',  ( -34.52287095715006160, -29.50250243563736774, 8.947779886222150481 ) ) ;
#97914=PLANE ( 'NONE',  #47460 ) ;
#97915=CARTESIAN_POINT ( 'NONE',  ( 14.04693994163893578, -13.95676237773968609, 11.49999999999998934 ) ) ;
#97917=CARTESIAN_POINT ( 'NONE',  ( 5.465678960246475704, -19.50585317057041124, 11.49999999999999645 ) ) ;
#97921=B_SPLINE_SURFACE_WITH_KNOTS ( 'NONE', 3, 3, ( 
 ( #70109, #21413, #38146, #91941 ),
 ( #61509, #92434, #23407, #84824 ),
 ( #52390, #83326, #6702, #13806 ),
 ( #99040, #44781, #68119, #91431 ),
 ( #54392, #46270, #69099, #99535 ),
 ( #69615, #97, #76206, #62002 ),
 ( #85321, #6204, #52890, #15812 ),
 ( #83829, #37656, #30032, #61007 ),
 ( #22411, #53394, #84322, #14804 ),
 ( #45771, #55398, #73486, #93939 ) ),
 .UNSPECIFIED., .F., .F., .F.,
 ( 4, 3, 3, 4 ),
 ( 4, 4 ),
 ( 0.7022005934544807149, 0.7765311282028797280, 0.8508616629512786300, 0.9995227324480766562 ),
 ( 0.8495965314205278229, 0.8511156036249712953 ),
 .UNSPECIFIED. ) ;
#97922=CARTESIAN_POINT ( 'NONE',  ( -88.88918693012689687, -29.50249591506787894, 5.947779886229223045 ) ) ;
#97923=DIRECTION ( 'NONE',  ( -3.773278334453079618E-23, 0.9999999999976377785, 2.173523156925979552E-06 ) ) ;
#97926=LINE ( 'NONE', #13690, #98128 ) ;
#97927=CARTESIAN_POINT ( 'NONE',  ( 7.329891291799937925, -18.66831812819665970, 11.49999999999998934 ) ) ;
#97928=CARTESIAN_POINT ( 'NONE',  ( -51.52287095715006870, -23.47596703998600631, 11.44779298504229104 ) ) ;
#97930=CARTESIAN_POINT ( 'NONE',  ( -41.26959558397305727, -25.07899898050004950, 7.338714981574760543 ) ) ;
#97931=B_SPLINE_CURVE_WITH_KNOTS ( 'NONE', 3,
 ( #94705, #40923, #94196, #71884, #25693, #24682 ),
 .UNSPECIFIED., .F., .F.,
 ( 4, 2, 4 ),
 ( 6.396512625966562883E-06, 0.001387752252890995597, 0.002769107993156024686 ),
 .UNSPECIFIED. ) ;
#97934=CARTESIAN_POINT ( 'NONE',  ( -89.55620429048339304, -23.47593901973091235, -1.443836447539002865 ) ) ;
#97936=CARTESIAN_POINT ( 'NONE',  ( -118.6228709571500701, -23.96177878511309345, 10.65340807706328974 ) ) ;
#97938=CARTESIAN_POINT ( 'NONE',  ( -14.39434090420295220, 17.20869321163716492, 11.49999999999999645 ) ) ;
#97939=CARTESIAN_POINT ( 'NONE',  ( -101.9714687704791487, -25.03707831087709934, 7.590867751134624086 ) ) ;
#97940=ORIENTED_EDGE ( 'NONE', *, *, #29992, .T. ) ;
#97941=CARTESIAN_POINT ( 'NONE',  ( 20.34676669208793953, -0.1217515720461415790, 11.49999999999998934 ) ) ;
#97942=ORIENTED_EDGE ( 'NONE', *, *, #84082, .T. ) ;
#97943=CARTESIAN_POINT ( 'NONE',  ( 6.461317529299694051, 22.01590093704556850, -1.500000000000002220 ) ) ;
#97947=CARTESIAN_POINT ( 'NONE',  ( -49.65594356225680173, -25.30517875835296593, 4.891185000421574891 ) ) ;
#97948=CARTESIAN_POINT ( 'NONE',  ( -77.55620429048342146, -24.64965694238574656, 8.947790433994196491 ) ) ;
#97950=CARTESIAN_POINT ( 'NONE',  ( -10.94853654022341516, 18.13385389444049522, 11.49999999999999645 ) ) ;
#97951=ORIENTED_EDGE ( 'NONE', *, *, #70853, .T. ) ;
#97953=CARTESIAN_POINT ( 'NONE',  ( -21.91774099701738621, 3.392077650570975766, 11.49999999999998934 ) ) ;
#97954=CARTESIAN_POINT ( 'NONE',  ( -3.210669876418242197, 20.33209092710186638, -1.500000000000002220 ) ) ;
#97955=EDGE_CURVE ( 'NONE', #67776, #63299, #71094, .T. ) ;
#97957=ORIENTED_EDGE ( 'NONE', *, *, #57037, .F. ) ;
#97959=CARTESIAN_POINT ( 'NONE',  ( -77.62287095715005592, -23.47593901973091235, -1.443836447539004642 ) ) ;
#97961=ORIENTED_EDGE ( 'NONE', *, *, #6288, .F. ) ;
#97964=CARTESIAN_POINT ( 'NONE',  ( -28.57980741741397068, -24.35756971646765479, 9.386484685950513551 ) ) ;
#97966=CARTESIAN_POINT ( 'NONE',  ( -2.730994233912177549, 20.60462238790213618, -1.500000000000002220 ) ) ;
#97967=CARTESIAN_POINT ( 'NONE',  ( 17.51545567653809954, -12.82042131148251229, 11.49999999999999645 ) ) ;
#97968=ORIENTED_EDGE ( 'NONE', *, *, #7498, .F. ) ;
#97969=CARTESIAN_POINT ( 'NONE',  ( -100.8391834046851159, -25.19504552050077706, 3.366519573641078011 ) ) ;
#97970=DIRECTION ( 'NONE',  ( -3.773278334453079618E-23, 0.9999999999976377785, 2.173523156925979975E-06 ) ) ;
#97971=CARTESIAN_POINT ( 'NONE',  ( -115.5161532992356967, -24.52300882791528380, 0.6510814631126371488 ) ) ;
#97972=CARTESIAN_POINT ( 'NONE',  ( -13.02831144489870319, 18.26546089674541307, 11.49999999999998934 ) ) ;
#97973=EDGE_CURVE ( 'NONE', #23684, #82501, #39630, .T. ) ;
#97976=CARTESIAN_POINT ( 'NONE',  ( -124.5228709571501042, -24.51387760970726504, 9.387446482453404073 ) ) ;
#97977=ORIENTED_EDGE ( 'NONE', *, *, #84803, .T. ) ;
#97978=CARTESIAN_POINT ( 'NONE',  ( -71.63953589603883643, -25.29442214193731076, 5.728881397446647483 ) ) ;
#97979=CARTESIAN_POINT ( 'NONE',  ( -129.5895376238167387, -24.64898659630367916, 1.056161002820393602 ) ) ;
#97980=ADVANCED_FACE ( 'NONE', ( #73126 ), #58226, .T. ) ;
#97982=EDGE_LOOP ( 'NONE', ( #71405, #94646, #19282, #89638 ) ) ;
#97983=ORIENTED_EDGE ( 'NONE', *, *, #95655, .T. ) ;
#97986=CARTESIAN_POINT ( 'NONE',  ( -12.29646723538143505, -17.35194501319736560, -1.500000000000002220 ) ) ;
#97987=ORIENTED_EDGE ( 'NONE', *, *, #17962, .T. ) ;
#97989=CARTESIAN_POINT ( 'NONE',  ( 9.711643268838683341, -19.58466107313252635, -1.500000000000002220 ) ) ;
#97990=FACE_OUTER_BOUND ( 'NONE', #30561, .T. ) ;
#97991=CARTESIAN_POINT ( 'NONE',  ( -2.919094682108430483, 22.50186656173435296, -1.500000000000002220 ) ) ;
#97992=CARTESIAN_POINT ( 'NONE',  ( -40.65892442973913745, -25.18430874473797942, 3.308410199191338386 ) ) ;
#97994=CARTESIAN_POINT ( 'NONE',  ( 15.04091035147580335, -15.99806323810862274, -1.500000000000002220 ) ) ;
#97995=CARTESIAN_POINT ( 'NONE',  ( -39.52287095715005449, -23.96127896941631619, -0.6493128931038099072 ) ) ;
#97996=VERTEX_POINT ( 'NONE', #97930 ) ;
#97998=ADVANCED_FACE ( 'NONE', ( #29930 ), #37550, .T. ) ;
#98000=DIRECTION ( 'NONE',  ( -3.773278334453080206E-23, 0.9999999999976377785, 2.173523156925979975E-06 ) ) ;
#98003=CARTESIAN_POINT ( 'NONE',  ( -18.72683625574626376, -10.08736549105613278, 11.49999999999998934 ) ) ;
#98004=CARTESIAN_POINT ( 'NONE',  ( -112.6245392106819452, -24.51314013834317151, 0.6176544820404282765 ) ) ;
#98006=VECTOR ( 'NONE', #13195, 1000.000000000000114 ) ;
#98008=CARTESIAN_POINT ( 'NONE',  ( -85.54470288293350677, -24.63355581998384736, 0.9682620441943965428 ) ) ;
#98009=CARTESIAN_POINT ( 'NONE',  ( -85.62287095715011276, -24.82576562982393042, 8.398263435472971494 ) ) ;
#98010=EDGE_CURVE ( 'NONE', #89989, #61715, #67502, .T. ) ;
#98013=CARTESIAN_POINT ( 'NONE',  ( 12.76379665850700640, 14.79237594083867080, 11.49999999999999645 ) ) ;
#98014=CARTESIAN_POINT ( 'NONE',  ( -109.3584176993576591, -25.27948031066536672, 4.206202526585778756 ) ) ;
#98016=EDGE_LOOP ( 'NONE', ( #99813, #95602, #416, #8983 ) ) ;
#98018=AXIS2_PLACEMENT_3D ( 'NONE', #9019, #33351, #70933 ) ;
#98019=CARTESIAN_POINT ( 'NONE',  ( -97.52287095715006160, -24.65952944569304606, 1.056160979905702346 ) ) ;
#98022=CARTESIAN_POINT ( 'NONE',  ( -63.52287095715006160, -23.47596703998600631, 11.44779298504228926 ) ) ;
#98023=EDGE_CURVE ( 'NONE', #79287, #100338, #38363, .T. ) ;
#98024=CARTESIAN_POINT ( 'NONE',  ( -106.5228709571500900, -24.34917612406837151, 0.1852690917426598749 ) ) ;
#98025=CARTESIAN_POINT ( 'NONE',  ( -6.535591236171724105, 18.61618873491671877, 11.49999999999998934 ) ) ;
#98027=ORIENTED_EDGE ( 'NONE', *, *, #13025, .F. ) ;
#98031=EDGE_CURVE ( 'NONE', #9929, #87827, #98928, .T. ) ;
#98033=VERTEX_POINT ( 'NONE', #32943 ) ;
#98035=CARTESIAN_POINT ( 'NONE',  ( -69.55620429048339304, -24.66019654487199020, 8.947790411086131712 ) ) ;
#98036=CARTESIAN_POINT ( 'NONE',  ( -105.2228709571501213, -23.47593901973090524, -1.443836447538997092 ) ) ;
#98037=CARTESIAN_POINT ( 'NONE',  ( -118.6289494624385696, -23.48783264082477018, -1.443836473390085695 ) ) ;
#98038=DIRECTION ( 'NONE',  ( 3.773278334444166432E-23, -1.000000000000000000, 0.000000000000000000 ) ) ;
#98039=DIRECTION ( 'NONE',  ( 0.000000000000000000, 0.9999999999976377785, 2.173523156925979128E-06 ) ) ;
#98040=B_SPLINE_CURVE_WITH_KNOTS ( 'NONE', 3,
 ( #32742, #63725, #25634, #87539, #48985, #79915 ),
 .UNSPECIFIED., .F., .F.,
 ( 4, 2, 4 ),
 ( 0.000000000000000000, 0.001380901958385392448, 0.002761803916770784895 ),
 .UNSPECIFIED. ) ;
#98041=CARTESIAN_POINT ( 'NONE',  ( -107.5199659751638706, -23.73766607897672642, -1.055555164236427590 ) ) ;
#98042=CARTESIAN_POINT ( 'NONE',  ( 0.05828707793547563409, -19.95834144014285272, 11.49999999999998934 ) ) ;
#98044=CARTESIAN_POINT ( 'NONE',  ( -0.01870951811792301994, -22.80779058525763148, 2.574493158953922389 ) ) ;
#98045=ORIENTED_EDGE ( 'NONE', *, *, #17346, .T. ) ;
#98046=CARTESIAN_POINT ( 'NONE',  ( -128.5562042904834072, -23.48786465467241413, 11.44779295918253226 ) ) ;
#98048=CARTESIAN_POINT ( 'NONE',  ( -119.5547944261018074, -24.15543982623907837, -0.2315651400026547124 ) ) ;
#98049=VECTOR ( 'NONE', #95445, 1000.000000000000114 ) ;
#98051=DIRECTION ( 'NONE',  ( -3.773278334453079030E-23, 0.9999999999976377785, 2.173523156925979128E-06 ) ) ;
#98052=CARTESIAN_POINT ( 'NONE',  ( -39.64153697460106685, -24.15543982623906416, -0.2315651400026677575 ) ) ;
#98054=CARTESIAN_POINT ( 'NONE',  ( -51.44554956638231147, -25.26280043022318367, 4.646412833070179715 ) ) ;
#98056=LINE ( 'NONE', #91950, #46274 ) ;
#98058=ORIENTED_EDGE ( 'NONE', *, *, #81577, .F. ) ;
#98059=CARTESIAN_POINT ( 'NONE',  ( -0.9278407348523283193, 20.21260682001012654, -1.500000000000002220 ) ) ;
#98060=CARTESIAN_POINT ( 'NONE',  ( -69.59881849519349828, -25.31566999480822489, 5.022752278581846141 ) ) ;
#98064=CARTESIAN_POINT ( 'NONE',  ( -79.06555067710175422, -25.31161594763374012, 5.326296773346069102 ) ) ;
#98065=DIRECTION ( 'NONE',  ( 0.000000000000000000, -2.173523156925979552E-06, 0.9999999999976378895 ) ) ;
#98066=CARTESIAN_POINT ( 'NONE',  ( -10.05502934987021391, 17.38067806581081598, -1.500000000000002220 ) ) ;
#98067=CARTESIAN_POINT ( 'NONE',  ( -13.78326148797977169, 15.88460234914768421, 11.49999999999999645 ) ) ;
#98068=CARTESIAN_POINT ( 'NONE',  ( -27.75915168180601000, -24.81617282942779923, 7.602034626381156457 ) ) ;
#98069=CARTESIAN_POINT ( 'NONE',  ( -70.65896739798220949, -23.48786465467241058, 11.44779295918254824 ) ) ;
#98070=CARTESIAN_POINT ( 'NONE',  ( -22.07534667767119174, -0.2742745133902674826, -1.500000000000002220 ) ) ;
#98071=VECTOR ( 'NONE', #80457, 1000.000000000000114 ) ;
#98072=LINE ( 'NONE', #90975, #70578 ) ;
#98076=VERTEX_POINT ( 'NONE', #40560 ) ;
#98077=CARTESIAN_POINT ( 'NONE',  ( -35.52287095715006870, -23.48786465467240347, 11.44779295918255180 ) ) ;
#98078=CARTESIAN_POINT ( 'NONE',  ( -31.66883481474841489, -23.48783264082477018, -1.443836473390079256 ) ) ;
#98079=EDGE_CURVE ( 'NONE', #22811, #82785, #52933, .T. ) ;
#98080=ORIENTED_EDGE ( 'NONE', *, *, #24132, .F. ) ;
#98081=ORIENTED_EDGE ( 'NONE', *, *, #88211, .T. ) ;
#98083=CARTESIAN_POINT ( 'NONE',  ( -93.52287095715006160, -24.66019654487200086, 8.947790411086110396 ) ) ;
#98085=CARTESIAN_POINT ( 'NONE',  ( -6.273408026305254737, 19.60348359158234288, -1.500000000000002220 ) ) ;
#98087=EDGE_CURVE ( 'NONE', #72503, #5107, #29921, .T. ) ;
#98088=CARTESIAN_POINT ( 'NONE',  ( 11.68953838083566588, 18.09531432177502808, 11.49999999999999645 ) ) ;
#98090=CARTESIAN_POINT ( 'NONE',  ( -50.33521035800622201, -25.13337234701628020, 7.100306106499248315 ) ) ;
#98091=CARTESIAN_POINT ( 'NONE',  ( -99.12380231474227799, -25.26431306044052150, 4.001575155705512366 ) ) ;
#98093=CARTESIAN_POINT ( 'NONE',  ( 3.003370282714790562, 22.13870467353671856, 11.49999999999998934 ) ) ;
#98098=CARTESIAN_POINT ( 'NONE',  ( -82.55620429048339304, -23.47593901973091235, -1.443836447539004642 ) ) ;
#98103=CARTESIAN_POINT ( 'NONE',  ( -5.628781154649386664, 20.11113626451368219, 11.49999999999998934 ) ) ;
#98104=ORIENTED_EDGE ( 'NONE', *, *, #60446, .F. ) ;
#98105=CARTESIAN_POINT ( 'NONE',  ( -40.43756433397305727, -25.11033443737753501, 2.832404817301930056 ) ) ;
#98106=ORIENTED_EDGE ( 'NONE', *, *, #36713, .T. ) ;
#98107=ORIENTED_EDGE ( 'NONE', *, *, #10912, .T. ) ;
#98108=CARTESIAN_POINT ( 'NONE',  ( -100.5484574693091986, -24.63419186844611275, 9.035850630976915099 ) ) ;
#98109=CARTESIAN_POINT ( 'NONE',  ( 7.532573551308565207, 19.69859070278346991, -1.500000000000002220 ) ) ;
#98112=CARTESIAN_POINT ( 'NONE',  ( -102.6228709571500559, -24.64965695001469115, 8.947790433994178727 ) ) ;
#98113=CARTESIAN_POINT ( 'NONE',  ( -108.5228709571500616, -29.50250786944525672, 11.44777988621622988 ) ) ;
#98114=CARTESIAN_POINT ( 'NONE',  ( -76.63418645068684043, -24.15620529776628089, 10.23563542870660470 ) ) ;
#98115=CARTESIAN_POINT ( 'NONE',  ( -50.06411376349647924, -25.11622845616857802, 2.865105794236846748 ) ) ;
#98116=CARTESIAN_POINT ( 'NONE',  ( -21.42251255223715134, 3.917230396363152067, -1.500000000000002220 ) ) ;
#98117=CARTESIAN_POINT ( 'NONE',  ( -72.52287095715007581, -29.50250243563736774, 8.947779886222143375 ) ) ;
#98118=CARTESIAN_POINT ( 'NONE',  ( -21.40455707349245529, -6.346402434563959361, 11.49999999999999645 ) ) ;
#98120=CARTESIAN_POINT ( 'NONE',  ( -116.5228709571501042, -23.47593901973090524, -1.443836447538996426 ) ) ;
#98122=EDGE_CURVE ( 'NONE', #12874, #93569, #54107, .T. ) ;
#98126=EDGE_CURVE ( 'NONE', #81255, #99009, #45652, .T. ) ;
#98128=VECTOR ( 'NONE', #82214, 1000.000000000000114 ) ;
#98132=EDGE_CURVE ( 'NONE', #94223, #33873, #77079, .T. ) ;
#98133=CARTESIAN_POINT ( 'NONE',  ( -47.62287095715004881, -29.50250243563736774, 8.947779886222146928 ) ) ;
#98134=FACE_OUTER_BOUND ( 'NONE', #38693, .T. ) ;
#98135=CARTESIAN_POINT ( 'NONE',  ( -86.52287095715006160, -29.50250243563736774, 8.947779886222139822 ) ) ;
#98136=ORIENTED_EDGE ( 'NONE', *, *, #51787, .F. ) ;
#98137=CARTESIAN_POINT ( 'NONE',  ( -9.862393454161701101, 16.67994275214481092, 11.49999999999999645 ) ) ;
#98139=ORIENTED_EDGE ( 'NONE', *, *, #78839, .F. ) ;
#98142=CARTESIAN_POINT ( 'NONE',  ( -116.5228709571500616, -24.64898659630368627, 1.056161002820833028 ) ) ;
#98143=DIRECTION ( 'NONE',  ( 3.773278334444167608E-23, -1.000000000000000000, 0.000000000000000000 ) ) ;
#98144=EDGE_CURVE ( 'NONE', #44615, #66922, #12923, .T. ) ;
#98145=CARTESIAN_POINT ( 'NONE',  ( 15.22544387773384500, -12.34335808662847178, -1.500000000000002220 ) ) ;
#98146=CARTESIAN_POINT ( 'NONE',  ( -37.52287095715006870, -24.64898659630367206, 1.056161002820819261 ) ) ;
#98147=VERTEX_POINT ( 'NONE', #19691 ) ;
#98148=CARTESIAN_POINT ( 'NONE',  ( -20.03152041342270806, -8.007337437543776915, 11.49999999999998934 ) ) ;
#98149=CARTESIAN_POINT ( 'NONE',  ( -33.62922567200806867, -24.51419770103157347, 9.386484678747185839 ) ) ;
#98150=CARTESIAN_POINT ( 'NONE',  ( -96.55620429048337883, -23.48783264082478439, -1.443836473390062380 ) ) ;
#98151=CARTESIAN_POINT ( 'NONE',  ( -81.55620429048336462, -24.64965694238574301, 8.947790433994203596 ) ) ;
#98153=CARTESIAN_POINT ( 'NONE',  ( -99.56269727232219680, -25.18439444651947312, 3.795001273127148078 ) ) ;
#98154=CARTESIAN_POINT ( 'NONE',  ( 12.94906671069258763, 19.00495796004926419, -1.500000000000002220 ) ) ;
#98156=B_SPLINE_CURVE_WITH_KNOTS ( 'NONE', 3,
 ( #35620, #82282, #12757, #13258 ),
 .UNSPECIFIED., .F., .F.,
 ( 4, 4 ),
 ( 0.9394548040336853090, 0.9404555510744508906 ),
 .UNSPECIFIED. ) ;
#98160=CARTESIAN_POINT ( 'NONE',  ( 9.931738293602487389, -17.53800358597336384, 11.49999999999999645 ) ) ;
#98164=VECTOR ( 'NONE', #64251, 1000.000000000000114 ) ;
#98165=PLANE ( 'NONE',  #47353 ) ;
#98167=CARTESIAN_POINT ( 'NONE',  ( -111.2787752023839971, -25.29779285926202803, 3.894639243670172668 ) ) ;
#98168=ADVANCED_FACE ( 'NONE', ( #87729 ), #52597, .T. ) ;
#98169=CARTESIAN_POINT ( 'NONE',  ( -14.63867168220055781, -13.42826565525684579, 11.49999999999998934 ) ) ;
#98170=B_SPLINE_CURVE_WITH_KNOTS ( 'NONE', 3,
 ( #89709, #20180, #59259, #20679, #13064, #27307, #58270, #36413, #67376, #19677, #50646, #36911, #89210, #81595 ),
 .UNSPECIFIED., .F., .F.,
 ( 4, 2, 2, 2, 2, 2, 4 ),
 ( 1.734723475976807094E-18, 0.0002000904627446527533, 0.0004001809254893037718, 0.0008003618509786153499, 0.001200542776467926820, 0.001400633239212573230, 0.001600723701957219424 ),
 .UNSPECIFIED. ) ;
#98171=VECTOR ( 'NONE', #82059, 1000.000000000000114 ) ;
#98172=CARTESIAN_POINT ( 'NONE',  ( -113.5949026862529507, -23.48783264082477018, -1.443836473390084363 ) ) ;
#98173=CARTESIAN_POINT ( 'NONE',  ( 14.45944668481935658, 13.51102189132778442, -1.500000000000002220 ) ) ;
#98174=AXIS2_PLACEMENT_3D ( 'NONE', #51307, #90861, #98460 ) ;
#98175=CARTESIAN_POINT ( 'NONE',  ( -126.5212060924008313, -24.15620529776629155, 10.23563542870658871 ) ) ;
#98176=CARTESIAN_POINT ( 'NONE',  ( -114.6228709571500701, -23.48783264082478794, -1.443836473390060382 ) ) ;
#98177=CARTESIAN_POINT ( 'NONE',  ( -66.55620429048340725, -23.47593901973091235, -1.443836447539006196 ) ) ;
#98178=CARTESIAN_POINT ( 'NONE',  ( 0.1934390699377774303, 20.68474938276070318, 11.49999999999999645 ) ) ;
#98179=CARTESIAN_POINT ( 'NONE',  ( -58.52287095715006160, -24.64898659630528499, 1.056161002820822592 ) ) ;
#98180=B_SPLINE_CURVE_WITH_KNOTS ( 'NONE', 3,
 ( #29745, #92135, #16503, #69808, #23109, #93129 ),
 .UNSPECIFIED., .F., .F.,
 ( 4, 2, 4 ),
 ( 1.570887131794638196E-05, 0.001396322306279762591, 0.002776935741241578874 ),
 .UNSPECIFIED. ) ;
#98183=CARTESIAN_POINT ( 'NONE',  ( 22.64978874513612439, 0.4204215919581203442, 11.49999999999999645 ) ) ;
#98185=CARTESIAN_POINT ( 'NONE',  ( -70.52287095715007581, -24.99156044556120548, 7.747789690856173195 ) ) ;
#98186=CARTESIAN_POINT ( 'NONE',  ( -42.58953762381672448, -23.47596703998600276, 11.44779298504227505 ) ) ;
#98187=DIRECTION ( 'NONE',  ( 3.773278334444167608E-23, -1.000000000000000000, 0.000000000000000000 ) ) ;
#98189=VERTEX_POINT ( 'NONE', #44545 ) ;
#98190=ORIENTED_EDGE ( 'NONE', *, *, #96283, .F. ) ;
#98191=CARTESIAN_POINT ( 'NONE',  ( -99.71988582849684235, -25.15588143334361249, 6.904968122648902806 ) ) ;
#98192=CARTESIAN_POINT ( 'NONE',  ( -17.76840699843883442, -14.40508365592194195, 11.49999999999998934 ) ) ;
#98194=CARTESIAN_POINT ( 'NONE',  ( -7.206546067468990735, 20.34698395366585189, -1.500000000000002220 ) ) ;
#98195=CARTESIAN_POINT ( 'NONE',  ( -113.5554261954940074, -23.96169478059713853, 10.65365249895717348 ) ) ;
#98196=CARTESIAN_POINT ( 'NONE',  ( -85.62287095715005592, -29.50250243563736774, 8.947779886222139822 ) ) ;
#98197=CARTESIAN_POINT ( 'NONE',  ( -5.352388609804938469, -21.92410630658433845, 11.49999999999999645 ) ) ;
#98199=CARTESIAN_POINT ( 'NONE',  ( -70.22848692110255797, -25.31612420714911238, 4.852864425714633612 ) ) ;
#98200=CARTESIAN_POINT ( 'NONE',  ( 21.99661117994144988, 0.4758108284031232760, 11.49999999999998934 ) ) ;
#98201=FACE_OUTER_BOUND ( 'NONE', #60982, .T. ) ;
#98203=ORIENTED_EDGE ( 'NONE', *, *, #47042, .T. ) ;
#98210=VERTEX_POINT ( 'NONE', #60283 ) ;
#98212=CARTESIAN_POINT ( 'NONE',  ( -65.52287095715006160, -23.47593901973090169, -1.443836447538996870 ) ) ;
#98213=DIRECTION ( 'NONE',  ( 1.000000000000000000, 3.773278334444166432E-23, 8.201307841325785021E-29 ) ) ;
#98215=CARTESIAN_POINT ( 'NONE',  ( -1.999887071766271784, 20.33596237858139233, -1.500000000000002220 ) ) ;
#98216=EDGE_CURVE ( 'NONE', #36438, #94640, #21190, .T. ) ;
#98219=CARTESIAN_POINT ( 'NONE',  ( -115.6228709571500985, -23.84081130438200802, 10.88220057463249191 ) ) ;
#98221=B_SPLINE_CURVE_WITH_KNOTS ( 'NONE', 3,
 ( #37624, #70077, #8180, #54864 ),
 .UNSPECIFIED., .F., .F.,
 ( 4, 4 ),
 ( 0.000000000000000000, 0.0001000000000000167422 ),
 .UNSPECIFIED. ) ;
#98222=CARTESIAN_POINT ( 'NONE',  ( -89.46310519935765626, -25.11033443737753856, 2.832404817301929612 ) ) ;
#98224=VERTEX_POINT ( 'NONE', #6976 ) ;
#98226=CARTESIAN_POINT ( 'NONE',  ( -28.27652290204276042, -24.63646046079093210, 8.166125576339837266 ) ) ;
#98227=ADVANCED_FACE ( 'NONE', ( #75972 ), #98757, .T. ) ;
#98228=CARTESIAN_POINT ( 'NONE',  ( 11.56195852851363526, -17.29799701895051811, 11.49999999999998934 ) ) ;
#98230=DIRECTION ( 'NONE',  ( -1.000000000000000000, -3.773278334444167608E-23, -8.201307833595939069E-29 ) ) ;
#98233=CARTESIAN_POINT ( 'NONE',  ( -28.62287095715006302, -23.79536559617938352, 10.65372852085395117 ) ) ;
#98234=DIRECTION ( 'NONE',  ( -0.000000000000000000, 2.173523156925979552E-06, -0.9999999999976378895 ) ) ;
#98236=ORIENTED_EDGE ( 'NONE', *, *, #91154, .F. ) ;
#98239=CARTESIAN_POINT ( 'NONE',  ( -119.2834285841887976, -25.28334328158019417, 4.245358510314063416 ) ) ;
#98242=CARTESIAN_POINT ( 'NONE',  ( -71.30358265130861639, -25.31201778570714822, 6.178525724323167267 ) ) ;
#98243=CARTESIAN_POINT ( 'NONE',  ( -13.50798789833325664, 17.53495777034937220, 11.49999999999999645 ) ) ;
#98245=VECTOR ( 'NONE', #20776, 1000.000000000000114 ) ;
#98246=CARTESIAN_POINT ( 'NONE',  ( -108.5200659837138915, -23.73766607897671221, -1.055555164236429144 ) ) ;
#98247=CARTESIAN_POINT ( 'NONE',  ( -8.787219534579676861, -20.84281209399103929, 11.49999999999998934 ) ) ;
#98250=ORIENTED_EDGE ( 'NONE', *, *, #11779, .T. ) ;
#98251=ORIENTED_EDGE ( 'NONE', *, *, #87511, .F. ) ;
#98252=CARTESIAN_POINT ( 'NONE',  ( -81.10288410982862217, -25.31541542150557689, 5.079550372627416266 ) ) ;
#98256=CARTESIAN_POINT ( 'NONE',  ( -4.481184387785930312, -21.81124396384582909, -1.500000000000002220 ) ) ;
#98257=B_SPLINE_CURVE_WITH_KNOTS ( 'NONE', 3,
 ( #38549, #23309, #69505, #85221, #61404, #15709 ),
 .UNSPECIFIED., .F., .F.,
 ( 4, 2, 4 ),
 ( 6.391158118972359742E-06, 0.001387004593080794169, 0.002767618028042615873 ),
 .UNSPECIFIED. ) ;
#98260=CARTESIAN_POINT ( 'NONE',  ( -97.62287095715005592, -24.64898659630367916, 1.056161002820829697 ) ) ;
#98262=LINE ( 'NONE', #28769, #31137 ) ;
#98263=AXIS2_PLACEMENT_3D ( 'NONE', #78499, #70915, #93730 ) ;
#98266=CARTESIAN_POINT ( 'NONE',  ( -1.849579639615634097, -19.42000222497389927, 11.49999999999998934 ) ) ;
#98267=CARTESIAN_POINT ( 'NONE',  ( -19.99255411920323056, 7.849732829375159149, -1.500000000000002220 ) ) ;
#98268=CARTESIAN_POINT ( 'NONE',  ( -25.81533462945560942, -24.57999804855655057, 3.045127745384520690 ) ) ;
#98270=CARTESIAN_POINT ( 'NONE',  ( -34.52287095715006160, -24.64898659630366851, 1.056161002820817485 ) ) ;
#98271=EDGE_CURVE ( 'NONE', #69448, #76836, #90218, .T. ) ;
#98272=B_SPLINE_CURVE_WITH_KNOTS ( 'NONE', 3,
 ( #67229, #60615, #99141, #19530 ),
 .UNSPECIFIED., .F., .F.,
 ( 4, 4 ),
 ( 0.6509648380567879533, 0.6599712693289033760 ),
 .UNSPECIFIED. ) ;
#98273=CARTESIAN_POINT ( 'NONE',  ( -0.7673284989158746239, 22.82873350090251918, -1.500000000000002220 ) ) ;
#98274=EDGE_CURVE ( 'NONE', #50179, #234, #31062, .T. ) ;
#98275=CARTESIAN_POINT ( 'NONE',  ( -39.52287095715006160, -24.50216790748204332, 0.6166512839542465096 ) ) ;
#98277=CARTESIAN_POINT ( 'NONE',  ( -2.986242917674419850, -19.73498743542299749, 11.49999999999999645 ) ) ;
#98278=CARTESIAN_POINT ( 'NONE',  ( -89.54303308397305727, -25.06732983082694943, 7.447789526168954843 ) ) ;
#98279=CARTESIAN_POINT ( 'NONE',  ( -123.6228709571500559, -23.72747288104441665, -1.053458166803660667 ) ) ;
#98281=EDGE_LOOP ( 'NONE', ( #55805, #39751, #35494, #62939 ) ) ;
#98282=CARTESIAN_POINT ( 'NONE',  ( -26.80331358727276836, -24.60615731223736802, 1.843589714496689957 ) ) ;
#98283=CARTESIAN_POINT ( 'NONE',  ( -68.52287095715006160, -24.64898659630528854, 1.056161002820824368 ) ) ;
#98284=CARTESIAN_POINT ( 'NONE',  ( 10.83000837110471082, 18.85367679709202804, -1.500000000000002220 ) ) ;
#98286=CARTESIAN_POINT ( 'NONE',  ( 7.829539893445508270, 17.95258299782629408, -1.500000000000002220 ) ) ;
#98287=AXIS2_PLACEMENT_3D ( 'NONE', #15181, #44644, #68972 ) ;
#98288=DIRECTION ( 'NONE',  ( -3.773278334453079030E-23, 0.9999999999976377785, 2.173523156925979128E-06 ) ) ;
#98289=EDGE_LOOP ( 'NONE', ( #94933, #29749, #35367, #12823 ) ) ;
#98291=CARTESIAN_POINT ( 'NONE',  ( -91.54409249466895915, -24.66019654487199730, 8.947790411086115725 ) ) ;
#98293=CARTESIAN_POINT ( 'NONE',  ( -13.21525772315781388, 15.71049578022273785, 11.49999999999999645 ) ) ;
#98296=DIRECTION ( 'NONE',  ( -3.773278334453079030E-23, 0.9999999999976377785, 2.173523156925979128E-06 ) ) ;
#98297=ORIENTED_EDGE ( 'NONE', *, *, #724, .T. ) ;
#98299=FACE_OUTER_BOUND ( 'NONE', #59208, .T. ) ;
#98301=CARTESIAN_POINT ( 'NONE',  ( -63.62287095715007723, -23.47596703998600631, 11.44779298504227683 ) ) ;
#98303=B_SPLINE_CURVE_WITH_KNOTS ( 'NONE', 3,
 ( #35239, #27630, #89516, #20001, #43356, #74293 ),
 .UNSPECIFIED., .F., .F.,
 ( 4, 2, 4 ),
 ( 0.000000000000000000, 0.001381509706665132392, 0.002763019413330264785 ),
 .UNSPECIFIED. ) ;
#98307=VECTOR ( 'NONE', #98296, 1000.000000000000114 ) ;
#98308=B_SPLINE_CURVE_WITH_KNOTS ( 'NONE', 3,
 ( #92124, #7382, #54086, #99718, #85007, #38338 ),
 .UNSPECIFIED., .F., .F.,
 ( 4, 2, 4 ),
 ( 6.391158118967745954E-06, 0.001387004593080787013, 0.002767618028042606333 ),
 .UNSPECIFIED. ) ;
#98309=B_SPLINE_CURVE_WITH_KNOTS ( 'NONE', 3,
 ( #10047, #87173, #54739, #62864, #70959, #24271 ),
 .UNSPECIFIED., .F., .F.,
 ( 4, 2, 4 ),
 ( 0.000000000000000000, 0.001380764517853247950, 0.002761529035706495900 ),
 .UNSPECIFIED. ) ;
#98311=CARTESIAN_POINT ( 'NONE',  ( -11.96207688724106610, 19.68918167733909641, 11.49999999999999645 ) ) ;
#98312=CARTESIAN_POINT ( 'NONE',  ( -4.239441843796335263, -22.36999388947090139, 11.49999999999998934 ) ) ;
#98313=CARTESIAN_POINT ( 'NONE',  ( -70.74026866089612042, -25.30458806305164643, 4.894904395092048333 ) ) ;
#98315=CARTESIAN_POINT ( 'NONE',  ( -49.51012166095222256, -25.26844836852635368, 3.931178963968652962 ) ) ;
#98316=CARTESIAN_POINT ( 'NONE',  ( -40.52287095715004739, -24.15516710230293995, 10.28746687063727450 ) ) ;
#98317=CARTESIAN_POINT ( 'NONE',  ( -99.16166289166535819, -25.31582281884252339, 5.311370716827876315 ) ) ;
#98318=CARTESIAN_POINT ( 'NONE',  ( -16.46405638241306946, -14.47283864684382237, 11.49999999999998934 ) ) ;
#98323=CARTESIAN_POINT ( 'NONE',  ( -60.24005634512300844, -25.33055341027920093, 4.734098254060623567 ) ) ;
#98325=EDGE_CURVE ( 'NONE', #73153, #98739, #17797, .T. ) ;
#98326=CARTESIAN_POINT ( 'NONE',  ( 2.691128592823461840, 20.25793168094256202, -1.500000000000002220 ) ) ;
#98327=ORIENTED_EDGE ( 'NONE', *, *, #1587, .F. ) ;
#98329=ORIENTED_EDGE ( 'NONE', *, *, #7869, .T. ) ;
#98330=ORIENTED_EDGE ( 'NONE', *, *, #60899, .F. ) ;
#98331=CARTESIAN_POINT ( 'NONE',  ( 23.03040035405544472, 1.057182387018521963, -1.500000000000002220 ) ) ;
#98332=CARTESIAN_POINT ( 'NONE',  ( -62.62287095715004881, -29.50250786944525672, 11.44777988621623876 ) ) ;
#98333=CARTESIAN_POINT ( 'NONE',  ( -5.148175472751820081, -19.54457232503198227, -1.500000000000002220 ) ) ;
#98334=EDGE_CURVE ( 'NONE', #76664, #87834, #10604, .T. ) ;
#98335=ORIENTED_EDGE ( 'NONE', *, *, #81969, .T. ) ;
#98336=VECTOR ( 'NONE', #50466, 1000.000000000000114 ) ;
#98337=FACE_OUTER_BOUND ( 'NONE', #51940, .T. ) ;
#98338=CARTESIAN_POINT ( 'NONE',  ( -116.6228709571500559, -29.50250786944525672, 11.44777988621622811 ) ) ;
#98339=ADVANCED_FACE ( 'NONE', ( #55170 ), #47049, .T. ) ;
#98340=CARTESIAN_POINT ( 'NONE',  ( -101.5228709571500190, -23.73934037231757088, 11.05740245334327909 ) ) ;
#98341=CARTESIAN_POINT ( 'NONE',  ( -53.61319971673114537, -23.48786465467240347, 11.44779295918255002 ) ) ;
#98342=CARTESIAN_POINT ( 'NONE',  ( -7.042111407433782055, -20.27750348750624099, 11.49999999999999645 ) ) ;
#98343=VERTEX_POINT ( 'NONE', #37925 ) ;
#98344=DIRECTION ( 'NONE',  ( -3.773278334444166432E-23, 1.000000000000000000, 0.000000000000000000 ) ) ;
#98345=ADVANCED_FACE ( 'NONE', ( #94202 ), #73608, .T. ) ;
#98346=ORIENTED_EDGE ( 'NONE', *, *, #94324, .T. ) ;
#98349=CARTESIAN_POINT ( 'NONE',  ( -16.63904852704994042, -12.34428335884295969, 11.49999999999998934 ) ) ;
#98351=B_SPLINE_CURVE_WITH_KNOTS ( 'NONE', 3,
 ( #4420, #49602, #56719, #87654 ),
 .UNSPECIFIED., .F., .F.,
 ( 4, 4 ),
 ( 0.000000000000000000, 9.999999999998897304E-05 ),
 .UNSPECIFIED. ) ;
#98352=CARTESIAN_POINT ( 'NONE',  ( -28.53660849338690042, -24.18923150054469318, 0.1864216068622559508 ) ) ;
#98353=ORIENTED_EDGE ( 'NONE', *, *, #75100, .F. ) ;
#98354=CARTESIAN_POINT ( 'NONE',  ( -61.52287095715006160, -24.66019654487199730, 8.947790411086121054 ) ) ;
#98355=VERTEX_POINT ( 'NONE', #3385 ) ;
#98356=CARTESIAN_POINT ( 'NONE',  ( -5.518977837361389582, -20.17201009624758257, -1.500000000000002220 ) ) ;
#98357=ADVANCED_FACE ( 'NONE', ( #87607 ), #3881, .T. ) ;
#98358=CARTESIAN_POINT ( 'NONE',  ( -18.59763704738199408, -11.70098744416181979, 11.49999999999999645 ) ) ;
#98359=CARTESIAN_POINT ( 'NONE',  ( -37.62372564847699152, -24.66019654487199730, 8.947790411086113949 ) ) ;
#98360=CARTESIAN_POINT ( 'NONE',  ( -6.671648801611133273, 21.52854475820963032, -1.500000000000002220 ) ) ;
#98362=CARTESIAN_POINT ( 'NONE',  ( -0.6469382494902750080, 20.97623560764392181, 11.49999999999998934 ) ) ;
#98363=CARTESIAN_POINT ( 'NONE',  ( -80.58953762381673869, -24.99132157543084531, 2.256160258750495640 ) ) ;
#98364=CARTESIAN_POINT ( 'NONE',  ( -29.52287095715006160, -29.50250473134420659, 10.00399446418115268 ) ) ;
#98369=CARTESIAN_POINT ( 'NONE',  ( -31.52287095715006160, -24.64965694238574656, 8.947790433994207149 ) ) ;
#98370=VECTOR ( 'NONE', #44676, 1000.000000000000114 ) ;
#98371=CARTESIAN_POINT ( 'NONE',  ( 8.645823604709390153, 19.67543227842514852, -1.500000000000002220 ) ) ;
#98374=CARTESIAN_POINT ( 'NONE',  ( -18.69274626484788371, 9.848020819832786543, 11.49999999999998934 ) ) ;
#98375=CARTESIAN_POINT ( 'NONE',  ( -71.20541289166536103, -25.30502758240210071, 4.885889971059796721 ) ) ;
#98376=CARTESIAN_POINT ( 'NONE',  ( -64.50492162725981871, -24.15543982623906416, -0.2315651400026674800 ) ) ;
#98377=CARTESIAN_POINT ( 'NONE',  ( -83.58528645688662095, -24.51419770103157347, 9.386484678747182286 ) ) ;
#98380=CARTESIAN_POINT ( 'NONE',  ( -99.20106123879247662, -25.22504103827928290, 3.603421885566837624 ) ) ;
#98381=CARTESIAN_POINT ( 'NONE',  ( 10.35204687333978057, 19.51823071965408829, -1.500000000000002220 ) ) ;
#98382=CARTESIAN_POINT ( 'NONE',  ( -116.5884090418037431, -24.51314013834316086, 0.6176544820404278324 ) ) ;
#98383=CARTESIAN_POINT ( 'NONE',  ( -51.90278039571972357, -25.24860200595528781, 5.898133925283090662 ) ) ;
#98384=CARTESIAN_POINT ( 'NONE',  ( -33.92287095715005307, -23.47593901973090169, -1.443836447538998202 ) ) ;
#98386=EDGE_CURVE ( 'NONE', #56311, #44968, #73507, .T. ) ;
#98387=CARTESIAN_POINT ( 'NONE',  ( -58.52287095715004739, -23.47593901973090169, -1.443836447538997092 ) ) ;
#98388=CARTESIAN_POINT ( 'NONE',  ( -16.98888496755095545, 9.415225082695979353, 11.49999999999998934 ) ) ;
#98389=CARTESIAN_POINT ( 'NONE',  ( -21.34312709018487553, 1.176582458498846462, -1.500000000000002220 ) ) ;
#98390=LINE ( 'NONE', #75053, #96871 ) ;
#98391=CARTESIAN_POINT ( 'NONE',  ( -61.52287095715006160, -23.48786465467241058, 11.44779295918254824 ) ) ;
#98394=CARTESIAN_POINT ( 'NONE',  ( -129.2228709571500644, -23.47593901973090524, -1.443836447538995982 ) ) ;
#98395=CARTESIAN_POINT ( 'NONE',  ( -17.13258802378025791, -14.77425600068537115, -1.500000000000002220 ) ) ;
#98396=ORIENTED_EDGE ( 'NONE', *, *, #44173, .F. ) ;
#98397=CARTESIAN_POINT ( 'NONE',  ( -128.5562042904834072, -24.65952944569305316, 1.056160979905707009 ) ) ;
#98398=CARTESIAN_POINT ( 'NONE',  ( -79.64682910312916420, -23.48783264082476308, -1.443836473390096575 ) ) ;
#98399=CARTESIAN_POINT ( 'NONE',  ( -9.134819693115781902, 17.59984377705169933, 11.49999999999999645 ) ) ;
#98401=CARTESIAN_POINT ( 'NONE',  ( -113.6228709571500559, -29.50248528299804818, 1.056150453629043584 ) ) ;
#98402=EDGE_LOOP ( 'NONE', ( #30692, #85855, #96863, #58830 ) ) ;
#98403=DIRECTION ( 'NONE',  ( -3.773278334453079030E-23, 0.9999999999976377785, 2.173523156925979128E-06 ) ) ;
#98404=CARTESIAN_POINT ( 'NONE',  ( -116.5228709571500616, -29.50250243563736774, 8.947779886222134493 ) ) ;
#98406=CARTESIAN_POINT ( 'NONE',  ( -2.642555958445479192, -21.45212208726272607, 11.49999999999998934 ) ) ;
#98409=CARTESIAN_POINT ( 'NONE',  ( 18.72033823704212097, 5.060218808788302880, -1.500000000000002220 ) ) ;
#98410=DIRECTION ( 'NONE',  ( -0.000000000000000000, 2.173523156925979552E-06, -0.9999999999976378895 ) ) ;
#98411=CARTESIAN_POINT ( 'NONE',  ( -61.52287095715006160, -29.50250243563736774, 8.947779886222145151 ) ) ;
#98412=CARTESIAN_POINT ( 'NONE',  ( 4.927431051831622000, -19.18327824014073357, -1.500000000000002220 ) ) ;
#98413=ORIENTED_EDGE ( 'NONE', *, *, #86793, .F. ) ;
#98414=AXIS2_PLACEMENT_3D ( 'NONE', #70833, #37880, #54608 ) ;
#98415=CARTESIAN_POINT ( 'NONE',  ( 17.42226438573850800, -10.51879874471254261, 11.49999999999999645 ) ) ;
#98419=ORIENTED_EDGE ( 'NONE', *, *, #53289, .F. ) ;
#98420=CARTESIAN_POINT ( 'NONE',  ( -102.5982595925881213, -23.48786465467241058, 11.44779295918254292 ) ) ;
#98424=CARTESIAN_POINT ( 'NONE',  ( -33.55620429048339304, -23.48783264082477373, -1.443836473390074593 ) ) ;
#98425=CARTESIAN_POINT ( 'NONE',  ( -17.52916707085001136, 9.785066945116392745, 11.49999999999998934 ) ) ;
#98426=CARTESIAN_POINT ( 'NONE',  ( -28.62287095715006302, -23.33147402473456822, -1.443835808584760683 ) ) ;
#98430=CARTESIAN_POINT ( 'NONE',  ( -5.953223121155255981, 22.05028593715628560, 11.49999999999999645 ) ) ;
#98431=CARTESIAN_POINT ( 'NONE',  ( -30.47287095715008221, -24.37837718399783782, 0.3290379132693308506 ) ) ;
#98432=CARTESIAN_POINT ( 'NONE',  ( -86.62287095715008434, -24.33832256526968862, 0.1851278514119904517 ) ) ;
#98438=CARTESIAN_POINT ( 'NONE',  ( 11.64234319522276095, -19.14997049866658330, 11.49999999999999645 ) ) ;
#98440=EDGE_LOOP ( 'NONE', ( #32740, #77643, #39367, #58177 ) ) ;
#98442=CARTESIAN_POINT ( 'NONE',  ( 15.61528876134825161, -13.05345633644532732, -1.500000000000002220 ) ) ;
#98445=CARTESIAN_POINT ( 'NONE',  ( 4.748521865011817944, 22.44708532425888592, 11.49999999999998934 ) ) ;
#98447=VERTEX_POINT ( 'NONE', #71387 ) ;
#98448=CARTESIAN_POINT ( 'NONE',  ( -60.52287095715006160, -23.47593901973090169, -1.443836447538996870 ) ) ;
#98450=CARTESIAN_POINT ( 'NONE',  ( -87.52287095715006160, -24.64898659630528854, 1.056161002820827921 ) ) ;
#98451=CARTESIAN_POINT ( 'NONE',  ( -12.22836702412972087, 17.35733969022439993, 11.49999999999999645 ) ) ;
#98453=ADVANCED_FACE ( 'NONE', ( #87097 ), #18579, .F. ) ;
#98455=CARTESIAN_POINT ( 'NONE',  ( 13.47465251475156656, -17.59220275312388182, -1.500000000000002220 ) ) ;
#98457=CARTESIAN_POINT ( 'NONE',  ( 0.06016934085327452914, 20.63536315578604174, 11.49999999999998934 ) ) ;
#98458=ORIENTED_EDGE ( 'NONE', *, *, #70625, .F. ) ;
#98459=ORIENTED_EDGE ( 'NONE', *, *, #8299, .F. ) ;
#98460=DIRECTION ( 'NONE',  ( -3.773278334444166432E-23, 1.000000000000000000, 0.000000000000000000 ) ) ;
#98462=ORIENTED_EDGE ( 'NONE', *, *, #51370, .T. ) ;
#98463=ORIENTED_EDGE ( 'NONE', *, *, #56668, .F. ) ;
#98465=CARTESIAN_POINT ( 'NONE',  ( -111.5920143885692539, -23.96169478059714564, 10.65365249895717348 ) ) ;
#98466=LINE ( 'NONE', #46197, #73039 ) ;
#98467=CARTESIAN_POINT ( 'NONE',  ( -19.91680486407696904, 5.911688619927280008, -1.500000000000002220 ) ) ;
#98469=CARTESIAN_POINT ( 'NONE',  ( -9.857415191643349672, 19.42730305858377449, 11.49999999999999645 ) ) ;
#98471=CARTESIAN_POINT ( 'NONE',  ( -39.50194508182622144, -25.25391041027802075, 3.881369232628720134 ) ) ;
#98472=CARTESIAN_POINT ( 'NONE',  ( -52.52287095715006160, -24.50216790748203621, 0.6166512839542510616 ) ) ;
#98473=AXIS2_PLACEMENT_3D ( 'NONE', #87665, #72946, #80545 ) ;
#98474=CARTESIAN_POINT ( 'NONE',  ( -115.6256605899217647, -24.63355581998384736, 0.9682620441943983192 ) ) ;
#98475=CARTESIAN_POINT ( 'NONE',  ( -13.02831144489870319, 18.26546089674541307, -1.500000000000002220 ) ) ;
#98477=VERTEX_POINT ( 'NONE', #40434 ) ;
#98479=CARTESIAN_POINT ( 'NONE',  ( -51.50945306740351981, -25.19752791585493412, 3.378729448321072137 ) ) ;
#98482=ORIENTED_EDGE ( 'NONE', *, *, #59686, .T. ) ;
#98483=CARTESIAN_POINT ( 'NONE',  ( -100.5248763468820528, -25.31387855574000412, 5.206551135935474584 ) ) ;
#98484=ORIENTED_EDGE ( 'NONE', *, *, #86238, .F. ) ;
#98485=CARTESIAN_POINT ( 'NONE',  ( 6.245503531335690361, -20.37428601906679759, -1.500000000000002220 ) ) ;
#98486=ORIENTED_EDGE ( 'NONE', *, *, #58101, .T. ) ;
#98488=CARTESIAN_POINT ( 'NONE',  ( -17.04133944854041616, 12.32129857345222845, -1.500000000000002220 ) ) ;
#98490=CARTESIAN_POINT ( 'NONE',  ( 16.14549698687068968, 15.95341496147077720, -1.500000000000002220 ) ) ;
#98492=CARTESIAN_POINT ( 'NONE',  ( -65.62287095715005592, -29.50250243563736774, 8.947779886222143375 ) ) ;
#98493=CARTESIAN_POINT ( 'NONE',  ( 15.10893391618534665, -15.86458014800626692, -1.500000000000002220 ) ) ;
#98494=PLANE ( 'NONE',  #94914 ) ;
#98496=CARTESIAN_POINT ( 'NONE',  ( -80.35919894935766195, -25.30543142107805465, 4.505481316334992492 ) ) ;
#98497=EDGE_CURVE ( 'NONE', #36479, #23202, #97765, .T. ) ;
#98498=VECTOR ( 'NONE', #7307, 1000.000000000000114 ) ;
#98499=ORIENTED_EDGE ( 'NONE', *, *, #5597, .T. ) ;
#98500=B_SPLINE_CURVE_WITH_KNOTS ( 'NONE', 3,
 ( #81829, #73716, #19427, #80836 ),
 .UNSPECIFIED., .F., .F.,
 ( 4, 4 ),
 ( 0.9504646280033649530, 0.9594710592754805978 ),
 .UNSPECIFIED. ) ;
#98502=CARTESIAN_POINT ( 'NONE',  ( -84.62359700266976859, -24.66019654487200441, 8.947790411086119278 ) ) ;
#98503=CARTESIAN_POINT ( 'NONE',  ( -130.5728709571500872, -25.30557784678704891, 3.856996771331003604 ) ) ;
#98504=CARTESIAN_POINT ( 'NONE',  ( -30.59902020641925446, -24.82963700391604078, 1.633150109380534509 ) ) ;
#98505=CARTESIAN_POINT ( 'NONE',  ( 6.361473516681357410, -20.28576754457002451, -1.500000000000002220 ) ) ;
#98506=DIRECTION ( 'NONE',  ( -3.773278334453079618E-23, 0.9999999999976377785, 2.173523156925979975E-06 ) ) ;
#98507=CARTESIAN_POINT ( 'NONE',  ( -26.92257395956520938, -24.75186024773817195, 2.526140358845352374 ) ) ;
#98508=CARTESIAN_POINT ( 'NONE',  ( -85.58560984767410673, -24.73486907724918282, 1.287355809206962576 ) ) ;
#98510=CARTESIAN_POINT ( 'NONE',  ( -70.52287095715010423, -24.14321612903118108, -0.2833117244520866329 ) ) ;
#98512=CARTESIAN_POINT ( 'NONE',  ( -79.62287095715007013, -23.95044443724992433, 10.65354141964649948 ) ) ;
#98513=VERTEX_POINT ( 'NONE', #64293 ) ;
#98514=DIRECTION ( 'NONE',  ( -3.773278334453080206E-23, 0.9999999999976377785, 2.173523156925979975E-06 ) ) ;
#98515=CARTESIAN_POINT ( 'NONE',  ( 16.09843989366402539, -11.26760994518913428, 11.49999999999999645 ) ) ;
#98516=CARTESIAN_POINT ( 'NONE',  ( -58.62287095715004881, -24.66019654487199020, 8.947790411086131712 ) ) ;
#98517=VECTOR ( 'NONE', #67623, 1000.000000000000114 ) ;
#98519=ORIENTED_EDGE ( 'NONE', *, *, #99643, .F. ) ;
#98520=CARTESIAN_POINT ( 'NONE',  ( -88.63180305775179590, -24.15620529776628800, 10.23563542870660115 ) ) ;
#98521=CARTESIAN_POINT ( 'NONE',  ( -40.62287095715005592, -23.47596703998600276, 11.44779298504227505 ) ) ;
#98522=CARTESIAN_POINT ( 'NONE',  ( -25.56040553771592627, -24.91036900288112932, 5.683877138022538134 ) ) ;
#98523=CARTESIAN_POINT ( 'NONE',  ( -31.62287095715005236, -29.50250786944525672, 11.44777988621624409 ) ) ;
#98524=CARTESIAN_POINT ( 'NONE',  ( -18.32884136524465291, -7.267937366463995907, -1.500000000000002220 ) ) ;
#98526=ORIENTED_EDGE ( 'NONE', *, *, #11340, .T. ) ;
#98528=CARTESIAN_POINT ( 'NONE',  ( -70.62287095715007013, -24.52232992886364116, 0.6492154411906061462 ) ) ;
#98529=EDGE_CURVE ( 'NONE', #61311, #40045, #68645, .T. ) ;
#98534=CARTESIAN_POINT ( 'NONE',  ( -55.58581373341920795, -24.63355581998385446, 0.9682620441943891043 ) ) ;
#98536=CARTESIAN_POINT ( 'NONE',  ( -31.62287095715005236, -24.50321055353803246, 9.387540953477538253 ) ) ;
#98538=CARTESIAN_POINT ( 'NONE',  ( -115.6228709571500559, -29.50249982740957577, 7.747779886224967605 ) ) ;
#98539=CARTESIAN_POINT ( 'NONE',  ( -85.62287095715007013, -25.00158670708909270, 2.256160236439165967 ) ) ;
#98540=CARTESIAN_POINT ( 'NONE',  ( 10.22567584263966722, 17.17405255344276682, 11.49999999999998934 ) ) ;
#98541=B_SPLINE_CURVE_WITH_KNOTS ( 'NONE', 3,
 ( #42767, #97037, #81313, #99012 ),
 .UNSPECIFIED., .F., .F.,
 ( 4, 4 ),
 ( 0.000000000000000000, 0.0001000000000000028644 ),
 .UNSPECIFIED. ) ;
#98542=CARTESIAN_POINT ( 'NONE',  ( -125.6228709571500559, -24.83620972994593501, 8.398175272781356782 ) ) ;
#98543=CARTESIAN_POINT ( 'NONE',  ( -0.02741748178391386140, -22.69505915253172645, 2.088213449219022078 ) ) ;
#98544=ORIENTED_EDGE ( 'NONE', *, *, #23411, .T. ) ;
#98545=EDGE_CURVE ( 'NONE', #62532, #39962, #66788, .T. ) ;
#98546=CARTESIAN_POINT ( 'NONE',  ( -116.5228709571500616, -23.47596703998600631, 11.44779298504227860 ) ) ;
#98549=CARTESIAN_POINT ( 'NONE',  ( -119.6235011850299941, -24.65952944569305316, 1.056160979905713226 ) ) ;
#98552=CARTESIAN_POINT ( 'NONE',  ( -39.55296486377296361, -23.96119346886879597, -0.6495511937832144644 ) ) ;
#98553=DIRECTION ( 'NONE',  ( -3.773278334453079618E-23, 0.9999999999976377785, 2.173523156925979975E-06 ) ) ;
#98554=B_SPLINE_CURVE_WITH_KNOTS ( 'NONE', 3,
 ( #24612, #78897, #71814, #85516 ),
 .UNSPECIFIED., .F., .F.,
 ( 4, 4 ),
 ( 1.387778780781445676E-17, 0.0001000000000000028508 ),
 .UNSPECIFIED. ) ;
#98555=CARTESIAN_POINT ( 'NONE',  ( -51.53844848903055009, -25.26280016857193544, 4.526031668297421540 ) ) ;
#98556=ORIENTED_EDGE ( 'NONE', *, *, #77018, .F. ) ;
#98557=B_SPLINE_SURFACE_WITH_KNOTS ( 'NONE', 3, 3, ( 
 ( #87895, #89392, #2670, #19865 ),
 ( #49350, #33607, #50839, #12248 ),
 ( #64590, #25991, #80279, #74168 ),
 ( #4664, #41737, #96500, #6644 ),
 ( #76146, #53337, #14749, #21359 ),
 ( #31873, #21855, #74656, #36103 ),
 ( #8531, #75156, #52827, #91877 ) ),
 .UNSPECIFIED., .F., .F., .F.,
 ( 4, 3, 4 ),
 ( 4, 4 ),
 ( 0.7945040050992245861, 0.8970133687736505657, 0.9995227324480765452 ),
 ( 0.8397073785246207400, 0.8411077677278031572 ),
 .UNSPECIFIED. ) ;
#98558=CARTESIAN_POINT ( 'NONE',  ( -34.62287095715005592, -24.34917612406837861, 0.1852690917426565997 ) ) ;
#98560=ORIENTED_EDGE ( 'NONE', *, *, #76160, .F. ) ;
#98561=CARTESIAN_POINT ( 'NONE',  ( -8.208445925564873846, -18.52556626786687488, 11.49999999999998934 ) ) ;
#98563=CARTESIAN_POINT ( 'NONE',  ( -122.5214661034149373, -23.73766607897671221, -1.055555164236450461 ) ) ;
#98566=LINE ( 'NONE', #12832, #49310 ) ;
#98567=ORIENTED_EDGE ( 'NONE', *, *, #77490, .T. ) ;
#98568=CARTESIAN_POINT ( 'NONE',  ( -94.92287095715005307, -23.47596703998600276, 11.44779298504227860 ) ) ;
#98569=PLANE ( 'NONE',  #85912 ) ;
#98570=CARTESIAN_POINT ( 'NONE',  ( 8.743921044546416610, -18.04861246754477477, -1.500000000000002220 ) ) ;
#98571=CARTESIAN_POINT ( 'NONE',  ( 6.686094007546604878, -20.02240253118446844, 11.49999999999999645 ) ) ;
#98572=DIRECTION ( 'NONE',  ( -3.773278334453079618E-23, 0.9999999999976377785, 2.173523156925979975E-06 ) ) ;
#98573=B_SPLINE_CURVE_WITH_KNOTS ( 'NONE', 3,
 ( #46798, #78718, #72146, #92951, #23426, #85344 ),
 .UNSPECIFIED., .F., .F.,
 ( 4, 2, 4 ),
 ( 6.391158118964604309E-06, 0.001387004593080783327, 0.002767618028042601996 ),
 .UNSPECIFIED. ) ;
#98574=CARTESIAN_POINT ( 'NONE',  ( -70.59200721846467275, -24.40133493613049964, 9.663955038902802386 ) ) ;
#98575=CARTESIAN_POINT ( 'NONE',  ( 0.6065052782250800467, 22.08157775750015617, 11.49999999999998934 ) ) ;
#98576=ADVANCED_FACE ( 'NONE', ( #20080 ), #29692, .F. ) ;
#98577=CARTESIAN_POINT ( 'NONE',  ( -20.35906544237474236, -2.577633573104691322, 11.49999999999998934 ) ) ;
#98578=DIRECTION ( 'NONE',  ( -1.000000000000000000, -3.773278334444166432E-23, -8.201307841325785021E-29 ) ) ;
#98579=CARTESIAN_POINT ( 'NONE',  ( -34.55620429048339304, -23.47593901973091235, -1.443836447539013301 ) ) ;
#98580=CARTESIAN_POINT ( 'NONE',  ( -69.62287095715005592, -24.64898659630528854, 1.056161002820824368 ) ) ;
#98581=ORIENTED_EDGE ( 'NONE', *, *, #16120, .F. ) ;
#98583=LINE ( 'NONE', #4754, #18652 ) ;
#98584=CARTESIAN_POINT ( 'NONE',  ( -102.5562042904833788, -23.47596703998600631, 11.44779298504227683 ) ) ;
#98587=ORIENTED_EDGE ( 'NONE', *, *, #60765, .F. ) ;
#98588=FACE_OUTER_BOUND ( 'NONE', #84715, .T. ) ;
#98590=CARTESIAN_POINT ( 'NONE',  ( -76.62361881388403617, -24.65952944569303895, 1.056160979905700792 ) ) ;
#98591=CARTESIAN_POINT ( 'NONE',  ( -20.44794078217315558, 2.270689272194197805, -1.500000000000002220 ) ) ;
#98592=EDGE_CURVE ( 'NONE', #25509, #78484, #15443, .T. ) ;
#98593=CARTESIAN_POINT ( 'NONE',  ( -18.50814150397365410, 11.09706937414969374, 11.49999999999999645 ) ) ;
#98594=VERTEX_POINT ( 'NONE', #89600 ) ;
#98595=PLANE ( 'NONE',  #61244 ) ;
#98596=CARTESIAN_POINT ( 'NONE',  ( -129.6228709571500133, -23.73907113216991860, -1.053371485793220375 ) ) ;
#98597=CARTESIAN_POINT ( 'NONE',  ( 9.556255610625576935, 20.19728179944524271, 11.49999999999998934 ) ) ;
#98599=CARTESIAN_POINT ( 'NONE',  ( -79.76746806413464697, -25.27875036686598165, 6.852562602421008009 ) ) ;
#98600=CARTESIAN_POINT ( 'NONE',  ( -84.60373966623234310, -23.48783264082476308, -1.443836473390094799 ) ) ;
#98601=ORIENTED_EDGE ( 'NONE', *, *, #99846, .T. ) ;
#98602=ADVANCED_FACE ( 'NONE', ( #36315 ), #89827, .T. ) ;
#98606=CARTESIAN_POINT ( 'NONE',  ( 20.66465755290784401, -3.126920214821775623, 11.49999999999998934 ) ) ;
#98608=CARTESIAN_POINT ( 'NONE',  ( -67.54911902231192755, -24.15620529776628800, 10.23563542870660115 ) ) ;
#98611=CARTESIAN_POINT ( 'NONE',  ( -50.80853080041594438, -25.30058970222920678, 4.652310615611309430 ) ) ;
#98612=CARTESIAN_POINT ( 'NONE',  ( 9.660767377612277329, -18.76748907076374095, -1.500000000000002220 ) ) ;
#98613=VERTEX_POINT ( 'NONE', #69756 ) ;
#98614=CARTESIAN_POINT ( 'NONE',  ( -117.5198302432919633, -23.96119346886881019, -0.6495511937831994764 ) ) ;
#98616=DIRECTION ( 'NONE',  ( 0.000000000000000000, 0.9999999999976377785, 2.173523156925979975E-06 ) ) ;
#98619=CARTESIAN_POINT ( 'NONE',  ( -12.70408864715453667, 17.69581422525067183, -1.500000000000002220 ) ) ;
#98620=FACE_OUTER_BOUND ( 'NONE', #69776, .T. ) ;
#98621=CARTESIAN_POINT ( 'NONE',  ( -15.13915969582853549, -16.40262476207453801, 11.49999999999999645 ) ) ;
#98623=PLANE ( 'NONE',  #40511 ) ;
#98628=EDGE_LOOP ( 'NONE', ( #99914, #35917, #82249, #49606 ) ) ;
#98629=CARTESIAN_POINT ( 'NONE',  ( -95.62287095715005592, -24.99156045073393173, 7.747789690856161648 ) ) ;
#98630=LINE ( 'NONE', #6292, #87090 ) ;
#98632=CARTESIAN_POINT ( 'NONE',  ( -13.43510958081001050, -13.94331287200543024, 11.49999999999998934 ) ) ;
#98634=ORIENTED_EDGE ( 'NONE', *, *, #43978, .T. ) ;
#98636=CARTESIAN_POINT ( 'NONE',  ( -18.68671320864135765, 5.291888989699490509, 11.49999999999999645 ) ) ;
#98638=AXIS2_PLACEMENT_3D ( 'NONE', #2265, #49443, #73271 ) ;
#98639=B_SPLINE_CURVE_WITH_KNOTS ( 'NONE', 3,
 ( #31826, #93210, #69384, #92705, #55177, #23194 ),
 .UNSPECIFIED., .F., .F.,
 ( 4, 2, 4 ),
 ( 6.384118678620645382E-06, 0.001386860460828382357, 0.002767336802978144061 ),
 .UNSPECIFIED. ) ;
#98641=CARTESIAN_POINT ( 'NONE',  ( -53.62287095715005592, -29.50247984919015209, -1.443849546365058689 ) ) ;
#98643=CARTESIAN_POINT ( 'NONE',  ( -102.6228709571500843, -24.51283580621365132, 0.6167428607019762588 ) ) ;
#98644=VECTOR ( 'NONE', #81528, 1000.000000000000114 ) ;
#98645=CARTESIAN_POINT ( 'NONE',  ( -130.5728709571500588, -24.04668586515358797, 10.47594215909545312 ) ) ;
#98646=CARTESIAN_POINT ( 'NONE',  ( -14.21210043416151159, 13.53504130633199765, 11.49999999999998934 ) ) ;
#98647=CARTESIAN_POINT ( 'NONE',  ( -46.50019354166188634, -24.15543982623906771, -0.2315651400026683127 ) ) ;
#98649=CARTESIAN_POINT ( 'NONE',  ( 21.55061338234859392, -0.003183148592148328428, -1.500000000000002220 ) ) ;
#98651=CARTESIAN_POINT ( 'NONE',  ( -33.59406827596458811, -24.15620529776627379, 10.23563542870661536 ) ) ;
#98652=CARTESIAN_POINT ( 'NONE',  ( -70.51930845923730828, -25.25639598314407408, 7.087032433890202654 ) ) ;
#98653=CARTESIAN_POINT ( 'NONE',  ( -40.52195335486641881, -23.48783264082477018, -1.443836473390102793 ) ) ;
#98654=CARTESIAN_POINT ( 'NONE',  ( -99.54260921963015107, -25.27473344898619700, 3.861216578678491995 ) ) ;
#98655=CARTESIAN_POINT ( 'NONE',  ( -22.04953120734539240, -6.464106996104416858, -1.500000000000002220 ) ) ;
#98656=B_SPLINE_CURVE_WITH_KNOTS ( 'NONE', 3,
 ( #65933, #49700, #88754, #96852, #80629, #65437 ),
 .UNSPECIFIED., .F., .F.,
 ( 4, 2, 4 ),
 ( 1.570887131794952276E-05, 0.001396322306279764325, 0.002776935741241578874 ),
 .UNSPECIFIED. ) ;
#98657=ADVANCED_FACE ( 'NONE', ( #37806 ), #16450, .T. ) ;
#98660=CARTESIAN_POINT ( 'NONE',  ( -88.92287095715005307, -23.47596703998600631, 11.44779298504227860 ) ) ;
#98661=CARTESIAN_POINT ( 'NONE',  ( -10.68008619461380704, -17.10268970254769982, 11.49999999999999645 ) ) ;
#98662=CARTESIAN_POINT ( 'NONE',  ( -45.62287095715004881, -24.51254535404255819, 9.355368623467651190 ) ) ;
#98665=DIRECTION ( 'NONE',  ( 0.000000000000000000, 0.9999999999976377785, 2.173523156925979975E-06 ) ) ;
#98666=CARTESIAN_POINT ( 'NONE',  ( -53.62287095715005592, -29.50250786944525672, 11.44777988621624054 ) ) ;
#98667=CARTESIAN_POINT ( 'NONE',  ( -38.58953762381673158, -24.64898659630528144, 1.056161002820817707 ) ) ;
#98668=CARTESIAN_POINT ( 'NONE',  ( 7.211006999188390942, 18.53272205163514030, 11.49999999999998934 ) ) ;
#98669=CARTESIAN_POINT ( 'NONE',  ( -82.62287095715005592, -24.64965695001468404, 8.947790433994182280 ) ) ;
#98670=EDGE_CURVE ( 'NONE', #89848, #21078, #2176, .T. ) ;
#98671=CARTESIAN_POINT ( 'NONE',  ( 18.46520180437041603, 7.126043738416648843, -1.500000000000002220 ) ) ;
#98672=ADVANCED_FACE ( 'NONE', ( #77841 ), #74434, .T. ) ;
#98673=CARTESIAN_POINT ( 'NONE',  ( -126.5905543067551946, -23.73791477778912551, 11.05961554403169878 ) ) ;
#98674=EDGE_CURVE ( 'NONE', #87827, #38848, #74746, .T. ) ;
#98679=CARTESIAN_POINT ( 'NONE',  ( -20.55277978778089576, -2.218614319624547360, 11.49999999999999645 ) ) ;
#98684=CARTESIAN_POINT ( 'NONE',  ( -19.63924127562733446, 11.44998032699685631, 11.49999999999999645 ) ) ;
#98686=CARTESIAN_POINT ( 'NONE',  ( -46.62287095715003460, -23.96177878511308634, 10.65340807706330217 ) ) ;
#98688=CARTESIAN_POINT ( 'NONE',  ( -9.895454706725905325, 17.58729670687104729, 11.49999999999998934 ) ) ;
#98689=EDGE_CURVE ( 'NONE', #56235, #49308, #88073, .T. ) ;
#98690=PLANE ( 'NONE',  #40298 ) ;
#98692=ORIENTED_EDGE ( 'NONE', *, *, #47865, .T. ) ;
#98693=B_SPLINE_CURVE_WITH_KNOTS ( 'NONE', 3,
 ( #71244, #1733, #32672, #62135, #46902, #86957 ),
 .UNSPECIFIED., .F., .F.,
 ( 4, 2, 4 ),
 ( 0.000000000000000000, 0.001380901958385390930, 0.002761803916770781860 ),
 .UNSPECIFIED. ) ;
#98694=B_SPLINE_CURVE_WITH_KNOTS ( 'NONE', 3,
 ( #99763, #45020, #44006, #74938 ),
 .UNSPECIFIED., .F., .F.,
 ( 4, 4 ),
 ( 0.000000000000000000, 9.999999999993348899E-05 ),
 .UNSPECIFIED. ) ;
#98698=CARTESIAN_POINT ( 'NONE',  ( 5.898633191892585614, -22.09092271590295198, -1.500000000000002220 ) ) ;
#98699=CARTESIAN_POINT ( 'NONE',  ( -29.62068022372628917, -23.40854978123364560, -1.443836171194816886 ) ) ;
#98700=CARTESIAN_POINT ( 'NONE',  ( 21.48638754631891246, 1.654510534108022179, -1.500000000000002220 ) ) ;
#98701=CARTESIAN_POINT ( 'NONE',  ( -59.62287095715004881, -29.50248528299804818, 1.056150453629034924 ) ) ;
#98703=CARTESIAN_POINT ( 'NONE',  ( -21.23328875057882570, -7.520457577684837247, 11.49999999999999645 ) ) ;
#98704=ORIENTED_EDGE ( 'NONE', *, *, #58109, .F. ) ;
#98705=CARTESIAN_POINT ( 'NONE',  ( -43.52287095715004028, -24.34917612407033616, 0.1852690917477757548 ) ) ;
#98706=CARTESIAN_POINT ( 'NONE',  ( 3.689792033372774060, 21.67897595795444587, 11.49999999999998934 ) ) ;
#98708=LINE ( 'NONE', #30191, #80281 ) ;
#98709=CARTESIAN_POINT ( 'NONE',  ( -99.62287095715005592, -29.50250243563736774, 8.947779886222138046 ) ) ;
#98710=ORIENTED_EDGE ( 'NONE', *, *, #61400, .F. ) ;
#98712=CARTESIAN_POINT ( 'NONE',  ( -90.51170739371271168, -24.15602025860896163, 10.28564288303535434 ) ) ;
#98713=EDGE_LOOP ( 'NONE', ( #13749, #54348, #83245, #41576 ) ) ;
#98714=PLANE ( 'NONE',  #72827 ) ;
#98717=VERTEX_POINT ( 'NONE', #34200 ) ;
#98719=CARTESIAN_POINT ( 'NONE',  ( -61.52287095715006160, -24.64898659630367916, 1.056161002820822592 ) ) ;
#98720=CARTESIAN_POINT ( 'NONE',  ( -104.5976497916026915, -23.48786465467241413, 11.44779295918254469 ) ) ;
#98721=CARTESIAN_POINT ( 'NONE',  ( 3.609400094169940676, -20.08663944828865766, -1.500000000000002220 ) ) ;
#98726=CARTESIAN_POINT ( 'NONE',  ( -65.62287095715005592, -29.50249982740957577, 7.747779886224967605 ) ) ;
#98727=EDGE_CURVE ( 'NONE', #18610, #41555, #83197, .T. ) ;
#98729=CARTESIAN_POINT ( 'NONE',  ( -51.52287095715006870, -24.64965694238407323, 8.947790433994203596 ) ) ;
#98730=ORIENTED_EDGE ( 'NONE', *, *, #89843, .F. ) ;
#98732=AXIS2_PLACEMENT_3D ( 'NONE', #7357, #252, #23575 ) ;
#98734=AXIS2_PLACEMENT_3D ( 'NONE', #76217, #95961, #18827 ) ;
#98735=CARTESIAN_POINT ( 'NONE',  ( 17.18838054715250152, -11.71887806637979779, -1.500000000000002220 ) ) ;
#98739=VERTEX_POINT ( 'NONE', #73262 ) ;
#98743=VERTEX_POINT ( 'NONE', #94585 ) ;
#98744=DIRECTION ( 'NONE',  ( -3.773278334453079618E-23, 0.9999999999976377785, 2.173523156925979975E-06 ) ) ;
#98745=PLANE ( 'NONE',  #67544 ) ;
#98746=CARTESIAN_POINT ( 'NONE',  ( -52.62287095715005592, -24.66019654487199020, 8.947790411086135265 ) ) ;
#98747=CARTESIAN_POINT ( 'NONE',  ( -61.62287095715004881, -24.64965695001468404, 8.947790433994185832 ) ) ;
#98748=CARTESIAN_POINT ( 'NONE',  ( -21.57569705560537088, 4.917917830663471435, 11.49999999999999645 ) ) ;
#98751=CARTESIAN_POINT ( 'NONE',  ( 3.867644355387967359, 22.30990608135428488, -1.500000000000002220 ) ) ;
#98753=EDGE_LOOP ( 'NONE', ( #71155, #79848, #50591, #97629 ) ) ;
#98756=CARTESIAN_POINT ( 'NONE',  ( -7.184633862932894743, 18.80532529184710100, -1.500000000000002220 ) ) ;
#98757=B_SPLINE_SURFACE_WITH_KNOTS ( 'NONE', 3, 1, ( 
 ( #6480, #98313 ),
 ( #67893, #89723 ),
 ( #52653, #28816 ),
 ( #20193, #51158 ),
 ( #43551, #68382 ) ),
 .UNSPECIFIED., .F., .F., .F.,
 ( 4, 1, 4 ),
 ( 2, 2 ),
 ( 0.000000000000000000, 0.5126593363417764060, 1.000000000000000000 ),
 ( 0.000000000000000000, 1.000000000000000000 ),
 .UNSPECIFIED. ) ;
#98759=ORIENTED_EDGE ( 'NONE', *, *, #43912, .F. ) ;
#98760=CARTESIAN_POINT ( 'NONE',  ( -40.41373532093560073, -25.30507957900415050, 5.542204897518816509 ) ) ;
#98761=CARTESIAN_POINT ( 'NONE',  ( 22.01400519847025450, -3.885951517071169370, -1.500000000000002220 ) ) ;
#98762=ORIENTED_EDGE ( 'NONE', *, *, #99366, .T. ) ;
#98763=ORIENTED_EDGE ( 'NONE', *, *, #38530, .T. ) ;
#98765=CARTESIAN_POINT ( 'NONE',  ( -89.62287095715004170, -23.47596703998600631, 11.44779298504227860 ) ) ;
#98766=CARTESIAN_POINT ( 'NONE',  ( -26.49992872176817826, -24.62748876299636436, 2.056831902527120004 ) ) ;
#98767=CARTESIAN_POINT ( 'NONE',  ( -99.62287095715005592, -24.64898659630367916, 1.056161002820829697 ) ) ;
#98768=CARTESIAN_POINT ( 'NONE',  ( 19.26631176993168282, 3.279242639417544236, -1.500000000000002220 ) ) ;
#98770=CARTESIAN_POINT ( 'NONE',  ( 11.86944616785735818, -17.87650476368427732, 11.49999999999998934 ) ) ;
#98771=CARTESIAN_POINT ( 'NONE',  ( -25.81533462945560942, -24.92774974205095972, 3.045126989538161855 ) ) ;
#98772=CARTESIAN_POINT ( 'NONE',  ( -108.6228709571500559, -29.50250243563736774, 8.947779886222136270 ) ) ;
#98773=CARTESIAN_POINT ( 'NONE',  ( -115.5895376238167387, -24.99132157543166954, 2.256160258750668390 ) ) ;
#98774=AXIS2_PLACEMENT_3D ( 'NONE', #31390, #8554, #62351 ) ;
#98775=CARTESIAN_POINT ( 'NONE',  ( 17.58993269669914383, -14.52173041563253975, -1.500000000000002220 ) ) ;
#98777=CARTESIAN_POINT ( 'NONE',  ( -96.62764419480109268, -24.35071581493543391, 9.817618358456023486 ) ) ;
#98778=PLANE ( 'NONE',  #83041 ) ;
#98779=CARTESIAN_POINT ( 'NONE',  ( 13.87436705529610492, 14.39054836566213780, 11.49999999999999645 ) ) ;
#98780=CARTESIAN_POINT ( 'NONE',  ( -111.5895376238167245, -23.47593901973091235, -1.443836447538999312 ) ) ;
#98781=EDGE_CURVE ( 'NONE', #7141, #91541, #14183, .T. ) ;
#98783=EDGE_CURVE ( 'NONE', #59400, #65117, #91642, .T. ) ;
#98784=DIRECTION ( 'NONE',  ( 1.000000000000000000, 3.773278334444167608E-23, 8.201307833595939069E-29 ) ) ;
#98785=DIRECTION ( 'NONE',  ( 3.773278334444167020E-23, -1.000000000000000000, 0.000000000000000000 ) ) ;
#98786=ORIENTED_EDGE ( 'NONE', *, *, #17875, .T. ) ;
#98788=CARTESIAN_POINT ( 'NONE',  ( -100.4381051993576364, -25.12049752546738191, 2.832404795212222215 ) ) ;
#98790=CARTESIAN_POINT ( 'NONE',  ( 10.83000837110471082, 18.85367679709202804, 11.49999999999998934 ) ) ;
#98793=CARTESIAN_POINT ( 'NONE',  ( 13.97609912898263573, 13.72534901313461653, -1.500000000000002220 ) ) ;
#98794=EDGE_CURVE ( 'NONE', #908, #35380, #8082, .T. ) ;
#98795=CARTESIAN_POINT ( 'NONE',  ( -99.77553290276979681, -25.16026440777957873, 6.940667289341870827 ) ) ;
#98800=CARTESIAN_POINT ( 'NONE',  ( -40.62287095715005592, -23.47596703998600276, 11.44779298504227505 ) ) ;
#98802=CARTESIAN_POINT ( 'NONE',  ( -1.764913036440812322, 20.45846032914734280, 11.49999999999999645 ) ) ;
#98803=CARTESIAN_POINT ( 'NONE',  ( -83.62287095715007013, -24.66019654487199730, 8.947790411086126383 ) ) ;
#98804=CARTESIAN_POINT ( 'NONE',  ( -42.55620429048337883, -24.66019654487199375, 8.947790411086135265 ) ) ;
#98806=ADVANCED_FACE ( 'NONE', ( #74250 ), #21436, .T. ) ;
#98807=ORIENTED_EDGE ( 'NONE', *, *, #16911, .T. ) ;
#98808=LINE ( 'NONE', #76961, #15135 ) ;
#98809=CARTESIAN_POINT ( 'NONE',  ( -84.52287095715006160, -29.50247984919015209, -1.443849546365053582 ) ) ;
#98810=LINE ( 'NONE', #67880, #75975 ) ;
#98813=FACE_OUTER_BOUND ( 'NONE', #89123, .T. ) ;
#98814=CARTESIAN_POINT ( 'NONE',  ( -12.06219892284564388, 19.56905390912838172, 11.49999999999999645 ) ) ;
#98815=CARTESIAN_POINT ( 'NONE',  ( -18.67006117854901959, 13.05921059288911934, 11.49999999999998934 ) ) ;
#98817=B_SPLINE_CURVE_WITH_KNOTS ( 'NONE', 3,
 ( #31068, #29577, #69138, #14842 ),
 .UNSPECIFIED., .F., .F.,
 ( 4, 4 ),
 ( 0.000000000000000000, 0.0001000000000000028644 ),
 .UNSPECIFIED. ) ;
#98819=CARTESIAN_POINT ( 'NONE',  ( -49.62291167701152261, -25.23900015727310020, 3.638722386798801445 ) ) ;
#98820=CARTESIAN_POINT ( 'NONE',  ( -40.52287095715009002, -23.85229601348996198, 10.88205029486209874 ) ) ;
#98821=CARTESIAN_POINT ( 'NONE',  ( -110.5518296883100362, -24.52300882791530512, 0.6510814631126329299 ) ) ;
#98822=CARTESIAN_POINT ( 'NONE',  ( 21.74639208212181529, -2.611101805624240768, 11.49999999999998934 ) ) ;
#98823=PLANE ( 'NONE',  #51103 ) ;
#98824=CARTESIAN_POINT ( 'NONE',  ( -87.55130102961774696, -24.15620529776628445, 10.23563542870660292 ) ) ;
#98826=CARTESIAN_POINT ( 'NONE',  ( -78.51253566907887205, -23.96119346886880308, -0.6495511937832113558 ) ) ;
#98827=CARTESIAN_POINT ( 'NONE',  ( -103.5895376238167103, -24.65952944569305316, 1.056160979905702790 ) ) ;
#98828=CARTESIAN_POINT ( 'NONE',  ( -86.62287095715004170, -24.64965695001468404, 8.947790433994180503 ) ) ;
#98829=ORIENTED_EDGE ( 'NONE', *, *, #97562, .T. ) ;
#98830=CARTESIAN_POINT ( 'NONE',  ( 11.41020680648336771, 16.95828056793917682, 11.49999999999998934 ) ) ;
#98832=ORIENTED_EDGE ( 'NONE', *, *, #16073, .T. ) ;
#98833=ORIENTED_EDGE ( 'NONE', *, *, #71117, .F. ) ;
#98835=CARTESIAN_POINT ( 'NONE',  ( -16.13607370526515794, 16.44073208242836159, 11.49999999999998934 ) ) ;
#98836=CARTESIAN_POINT ( 'NONE',  ( -35.52287095715006160, -23.85196035787604174, -0.8779234886343784128 ) ) ;
#98837=CARTESIAN_POINT ( 'NONE',  ( -12.21837793623082113, -16.16665877782589433, -1.500000000000002220 ) ) ;
#98838=ORIENTED_EDGE ( 'NONE', *, *, #68557, .F. ) ;
#98839=CARTESIAN_POINT ( 'NONE',  ( -28.20653904363605236, -25.02819912641725963, 6.759032221908313431 ) ) ;
#98840=CARTESIAN_POINT ( 'NONE',  ( -87.62287095715004170, -24.66019654487199020, 8.947790411086129936 ) ) ;
#98841=EDGE_CURVE ( 'NONE', #21630, #63898, #59532, .T. ) ;
#98842=CARTESIAN_POINT ( 'NONE',  ( -89.81226385320383088, -25.27367468601175204, 3.993462154588550916 ) ) ;
#98843=CARTESIAN_POINT ( 'NONE',  ( -70.51358761491228222, -23.85016227208580730, -0.8807180028928335291 ) ) ;
#98844=CARTESIAN_POINT ( 'NONE',  ( 21.40653236543258231, -1.377805879665675803, 11.49999999999999645 ) ) ;
#98847=CARTESIAN_POINT ( 'NONE',  ( -41.48142716432091248, -24.65952944569304606, 1.056160979905696351 ) ) ;
#98848=EDGE_LOOP ( 'NONE', ( #34548, #44080, #99228, #51574 ) ) ;
#98849=CARTESIAN_POINT ( 'NONE',  ( 2.909938941155331360, -20.50406750007545398, 11.49999999999998934 ) ) ;
#98850=VECTOR ( 'NONE', #49452, 1000.000000000000114 ) ;
#98852=B_SPLINE_CURVE_WITH_KNOTS ( 'NONE', 3,
 ( #13379, #100094, #76275, #44359 ),
 .UNSPECIFIED., .F., .F.,
 ( 4, 4 ),
 ( 0.01980006321810323308, 0.02880649449021864886 ),
 .UNSPECIFIED. ) ;
#98854=CARTESIAN_POINT ( 'NONE',  ( -28.57182946747713359, -23.32753131072699304, -1.443835813551990865 ) ) ;
#98859=CARTESIAN_POINT ( 'NONE',  ( -5.413507703253908510, 20.27406835261982465, -1.500000000000002220 ) ) ;
#98860=CARTESIAN_POINT ( 'NONE',  ( 1.885617179787854036, 21.85875792104173598, 11.49999999999999645 ) ) ;
#98862=VECTOR ( 'NONE', #65535, 1000.000000000000114 ) ;
#98863=CARTESIAN_POINT ( 'NONE',  ( 22.10748686624256720, -4.471405416651531795, 11.49999999999998934 ) ) ;
#98864=CARTESIAN_POINT ( 'NONE',  ( -16.09219062524700661, 13.46031615953476468, 11.49999999999998934 ) ) ;
#98865=CARTESIAN_POINT ( 'NONE',  ( -111.5228709571500616, -24.64898659630368627, 1.056161002820831474 ) ) ;
#98866=CARTESIAN_POINT ( 'NONE',  ( -96.62287095715005592, -29.50248528299804818, 1.056150453629042030 ) ) ;
#98872=ORIENTED_EDGE ( 'NONE', *, *, #48098, .T. ) ;
#98873=CARTESIAN_POINT ( 'NONE',  ( -66.64100815734259697, -23.96119346886880308, -0.6495511937832151306 ) ) ;
#98874=B_SPLINE_CURVE_WITH_KNOTS ( 'NONE', 3,
 ( #95741, #25727, #56703, #19605, #26731, #51072, #27730, #10000, #18606, #2912, #96247, #66313, #50079, #33841, #42475, #88636 ),
 .UNSPECIFIED., .F., .F.,
 ( 4, 2, 2, 2, 2, 2, 2, 4 ),
 ( 7.059813062317230268E-18, 0.0002422919684164868688, 0.0004845839368329666903, 0.0009691678736659256827, 0.001211459842082404908, 0.001453751810498883808, 0.001696043778915362924, 0.001938335747331841824 ),
 .UNSPECIFIED. ) ;
#98875=VECTOR ( 'NONE', #5297, 1000.000000000000114 ) ;
#98876=CARTESIAN_POINT ( 'NONE',  ( -7.320277434469578459, 20.25297033093062282, -1.500000000000002220 ) ) ;
#98880=CARTESIAN_POINT ( 'NONE',  ( 1.943494986365726485, -21.02143711168614004, -1.500000000000002220 ) ) ;
#98882=CARTESIAN_POINT ( 'NONE',  ( -130.2562042904833675, -23.47593901973090524, -1.443836447538995982 ) ) ;
#98883=CARTESIAN_POINT ( 'NONE',  ( -83.55086462815660298, -24.15620529776628089, 10.23563542870660470 ) ) ;
#98885=CARTESIAN_POINT ( 'NONE',  ( -99.30982394651951495, -25.19814257758587672, 3.382988130124507276 ) ) ;
#98886=CARTESIAN_POINT ( 'NONE',  ( 2.303347834742990763, 21.97011321758780866, -1.500000000000002220 ) ) ;
#98887=CARTESIAN_POINT ( 'NONE',  ( -30.48634990730260341, -23.47593902148418010, -1.443029787961928267 ) ) ;
#98889=CARTESIAN_POINT ( 'NONE',  ( -109.2061753004840057, -25.30575712527984678, 4.991482944917066789 ) ) ;
#98890=CARTESIAN_POINT ( 'NONE',  ( -79.62287095715004170, -24.50216790748205042, 0.6166512839542579449 ) ) ;
#98891=CARTESIAN_POINT ( 'NONE',  ( -57.62287095715004881, -29.50250243563736774, 8.947779886222145151 ) ) ;
#98892=CARTESIAN_POINT ( 'NONE',  ( -100.5972946370290231, -23.85016227208580020, -0.8807180028928295323 ) ) ;
#98893=CARTESIAN_POINT ( 'NONE',  ( -7.106217341473486826, 18.08270997100935418, -1.500000000000002220 ) ) ;
#98894=CARTESIAN_POINT ( 'NONE',  ( 20.27498964588844643, 6.839650151297337999, 11.49999999999998934 ) ) ;
#98895=CARTESIAN_POINT ( 'NONE',  ( -26.09764195947040477, -24.97014115428614289, 5.074844938448132226 ) ) ;
#98896=CARTESIAN_POINT ( 'NONE',  ( -81.58953762381672448, -23.48786465467241058, 11.44779295918254647 ) ) ;
#98897=CARTESIAN_POINT ( 'NONE',  ( -108.8968792378191921, -25.05712065398430966, 7.447789548358837663 ) ) ;
#98899=CARTESIAN_POINT ( 'NONE',  ( 20.48348528492645571, -9.684159049092739835, -1.500000000000002220 ) ) ;
#98900=ORIENTED_EDGE ( 'NONE', *, *, #52589, .F. ) ;
#98903=CARTESIAN_POINT ( 'NONE',  ( 16.85830656838225039, -10.38424343889589707, 11.49999999999999645 ) ) ;
#98904=ADVANCED_FACE ( 'NONE', ( #44311 ), #98569, .F. ) ;
#98906=ORIENTED_EDGE ( 'NONE', *, *, #6081, .F. ) ;
#98908=EDGE_CURVE ( 'NONE', #71598, #39801, #50313, .T. ) ;
#98909=CARTESIAN_POINT ( 'NONE',  ( -87.62287095715004170, -23.47596703998600631, 11.44779298504227860 ) ) ;
#98910=CARTESIAN_POINT ( 'NONE',  ( 9.069627533930374241, 19.64968329815391712, 11.49999999999998934 ) ) ;
#98911=CARTESIAN_POINT ( 'NONE',  ( -27.30764964498456138, -24.78236438415111564, 7.550007144492702160 ) ) ;
#98912=CARTESIAN_POINT ( 'NONE',  ( -4.539579955115475407, -18.87035741768621122, -1.500000000000002220 ) ) ;
#98914=CARTESIAN_POINT ( 'NONE',  ( -80.52287095715006160, -23.48786465467241769, 11.44779295918254469 ) ) ;
#98915=CARTESIAN_POINT ( 'NONE',  ( -129.5228709571501327, -24.33927499327856125, 9.819080762295810061 ) ) ;
#98916=CARTESIAN_POINT ( 'NONE',  ( 1.944447714513537262, -19.71154682592685958, -1.500000000000002220 ) ) ;
#98919=CARTESIAN_POINT ( 'NONE',  ( 19.78452974690265975, -4.759501717958375622, 11.49999999999999645 ) ) ;
#98920=DIRECTION ( 'NONE',  ( -3.773278334444166432E-23, 1.000000000000000000, 0.000000000000000000 ) ) ;
#98921=EDGE_CURVE ( 'NONE', #58188, #44485, #93964, .T. ) ;
#98922=VECTOR ( 'NONE', #6892, 1000.000000000000114 ) ;
#98925=CARTESIAN_POINT ( 'NONE',  ( -102.5490346760724947, -24.51419770103155926, 9.386484678747178734 ) ) ;
#98926=DIRECTION ( 'NONE',  ( -3.773278334444166432E-23, 1.000000000000000000, 0.000000000000000000 ) ) ;
#98928=B_SPLINE_CURVE_WITH_KNOTS ( 'NONE', 3,
 ( #67510, #68998, #76592, #98431, #99922, #29426, #22305, #28935, #90835, #21308, #52279, #83215, #75592, #55293, #9098, #86223, #9600, #93834, #63917, #62395, #24320, #7596, #16706, #79101, #47674, #48173 ),
 .UNSPECIFIED., .F., .F.,
 ( 4, 2, 2, 2, 2, 2, 2, 2, 2, 2, 2, 2, 4 ),
 ( 2.071553103015771015E-05, 0.001703922715423791898, 0.002545526307620607151, 0.003387129899817422404, 0.004228733492014237656, 0.005070337084211053343, 0.006753544268604682113, 0.007595147860801496932, 0.008436751452998311751, 0.01011995863739193965, 0.01096156222958875708, 0.01180316582178557276, 0.01348637300617921107 ),
 .UNSPECIFIED. ) ;
#98929=DIRECTION ( 'NONE',  ( -3.773278334453079030E-23, 0.9999999999976377785, 2.173523156925979128E-06 ) ) ;
#98930=B_SPLINE_CURVE_WITH_KNOTS ( 'NONE', 3,
 ( #16603, #10002, #64831, #2404 ),
 .UNSPECIFIED., .F., .F.,
 ( 4, 4 ),
 ( 0.000000000000000000, 9.999999999998897304E-05 ),
 .UNSPECIFIED. ) ;
#98931=B_SPLINE_CURVE_WITH_KNOTS ( 'NONE', 3,
 ( #26516, #88415, #58473, #5168 ),
 .UNSPECIFIED., .F., .F.,
 ( 4, 4 ),
 ( 0.000000000000000000, 1.000000000000000000 ),
 .UNSPECIFIED. ) ;
#98932=CARTESIAN_POINT ( 'NONE',  ( -51.46188133747676119, -25.21125483986890004, 6.515194751273123863 ) ) ;
#98933=CARTESIAN_POINT ( 'NONE',  ( -6.237196068801617699, -19.06703463882530158, 11.49999999999998934 ) ) ;
#98937=CARTESIAN_POINT ( 'NONE',  ( -93.58953762381672448, -24.66019654487199730, 8.947790411086121054 ) ) ;
#98938=CARTESIAN_POINT ( 'NONE',  ( -2.657479817400386413, -22.66247145590962120, 11.49999999999999645 ) ) ;
#98944=PLANE ( 'NONE',  #94835 ) ;
#98945=DIRECTION ( 'NONE',  ( -3.773278334453079030E-23, 0.9999999999976377785, 2.173523156925979128E-06 ) ) ;
#98947=CARTESIAN_POINT ( 'NONE',  ( 12.22771034161782566, -16.27230226814707947, 11.49999999999998934 ) ) ;
#98948=ORIENTED_EDGE ( 'NONE', *, *, #50345, .T. ) ;
#98949=ADVANCED_FACE ( 'NONE', ( #43312 ), #13831, .F. ) ;
#98950=CARTESIAN_POINT ( 'NONE',  ( 14.22603995551189371, 18.00578905361294346, -1.500000000000002220 ) ) ;
#98951=FACE_OUTER_BOUND ( 'NONE', #46468, .T. ) ;
#98952=ORIENTED_EDGE ( 'NONE', *, *, #67777, .F. ) ;
#98953=LINE ( 'NONE', #23322, #59096 ) ;
#98954=CARTESIAN_POINT ( 'NONE',  ( -72.52287095715007581, -29.50250786944525672, 11.44777988621623699 ) ) ;
#98956=CARTESIAN_POINT ( 'NONE',  ( -40.62287095715007723, -24.82558206586143257, 1.605769216559447266 ) ) ;
#98957=CARTESIAN_POINT ( 'NONE',  ( -9.338289970059909351, 19.12570833482435617, 11.49999999999999645 ) ) ;
#98958=VERTEX_POINT ( 'NONE', #87233 ) ;
#98960=CARTESIAN_POINT ( 'NONE',  ( 14.71430157977438924, -16.63553917435140406, -1.500000000000002220 ) ) ;
#98961=CARTESIAN_POINT ( 'NONE',  ( -13.12974562303265813, -15.89414520977026513, -1.500000000000002220 ) ) ;
#98962=ORIENTED_EDGE ( 'NONE', *, *, #94154, .T. ) ;
#98965=EDGE_CURVE ( 'NONE', #56669, #89809, #41882, .T. ) ;
#98966=CARTESIAN_POINT ( 'NONE',  ( -39.98487219060604048, -25.13257598017197836, 2.899846256276811918 ) ) ;
#98968=ORIENTED_EDGE ( 'NONE', *, *, #12082, .T. ) ;
#98970=CARTESIAN_POINT ( 'NONE',  ( -41.59371021311409322, -24.15620529776627379, 10.23563542870660825 ) ) ;
#98971=CARTESIAN_POINT ( 'NONE',  ( 5.313885144808909722, 20.14914662543312929, -1.500000000000002220 ) ) ;
#98972=CARTESIAN_POINT ( 'NONE',  ( 12.66963027563507005, -17.75133666976559255, 11.49999999999999645 ) ) ;
#98973=EDGE_CURVE ( 'NONE', #63463, #36561, #26245, .T. ) ;
#98974=CARTESIAN_POINT ( 'NONE',  ( -50.50582907151566303, -25.03335633882959144, 7.560799548800013703 ) ) ;
#98975=CARTESIAN_POINT ( 'NONE',  ( -113.6228709571501412, -24.35013146730204525, 9.818937971375106599 ) ) ;
#98976=CARTESIAN_POINT ( 'NONE',  ( -17.72129891523481149, -13.73837202384828515, 11.49999999999998934 ) ) ;
#98978=EDGE_LOOP ( 'NONE', ( #8255, #52875, #52603, #68947 ) ) ;
#98979=CARTESIAN_POINT ( 'NONE',  ( -71.70647007306178011, -25.26304665851990094, 6.133561479734631838 ) ) ;
#98980=FACE_OUTER_BOUND ( 'NONE', #5449, .T. ) ;
#98981=ORIENTED_EDGE ( 'NONE', *, *, #22624, .F. ) ;
#98982=ORIENTED_EDGE ( 'NONE', *, *, #48299, .F. ) ;
#98984=DIRECTION ( 'NONE',  ( 3.773278334444167608E-23, -1.000000000000000000, 0.000000000000000000 ) ) ;
#98986=ORIENTED_EDGE ( 'NONE', *, *, #84970, .F. ) ;
#98987=CARTESIAN_POINT ( 'NONE',  ( 10.72677997844354536, -18.41129465587203740, -1.500000000000002220 ) ) ;
#98990=CARTESIAN_POINT ( 'NONE',  ( -20.73700405699343463, 3.470425206167693233, -1.500000000000002220 ) ) ;
#98991=CARTESIAN_POINT ( 'NONE',  ( -45.55620429048339304, -23.48783264082477373, -1.443836473390068820 ) ) ;
#98993=CARTESIAN_POINT ( 'NONE',  ( -79.11611000704996854, -25.20074463982482982, 3.409327697717700278 ) ) ;
#98994=CARTESIAN_POINT ( 'NONE',  ( -9.563806973793814947, 19.74097577964120376, -1.500000000000002220 ) ) ;
#98995=CARTESIAN_POINT ( 'NONE',  ( -52.62287095715005592, -29.50250243563736774, 8.947779886222146928 ) ) ;
#98996=ORIENTED_EDGE ( 'NONE', *, *, #72821, .T. ) ;
#98997=CARTESIAN_POINT ( 'NONE',  ( -80.80267296708018421, -25.30788629407443935, 4.569020114890182782 ) ) ;
#98998=CARTESIAN_POINT ( 'NONE',  ( -84.54195721757037063, -24.66019654487200441, 8.947790411086115725 ) ) ;
#98999=VECTOR ( 'NONE', #12921, 1000.000000000000114 ) ;
#99000=CARTESIAN_POINT ( 'NONE',  ( -130.5728709571501156, -25.30559561715419647, 6.147794833475638931 ) ) ;
#99001=CARTESIAN_POINT ( 'NONE',  ( -0.1490749075164066184, -21.12010817310450861, 11.44779298504228038 ) ) ;
#99002=CARTESIAN_POINT ( 'NONE',  ( 15.78869406909177897, -14.30566568001193950, -1.500000000000002220 ) ) ;
#99003=CARTESIAN_POINT ( 'NONE',  ( -98.58873755195853050, -24.35071581493543746, 9.817618358456027039 ) ) ;
#99004=CARTESIAN_POINT ( 'NONE',  ( -27.61766922344000363, -24.75185970960561122, 2.278554975841372787 ) ) ;
#99005=CARTESIAN_POINT ( 'NONE',  ( -61.22287095715005023, -23.47596703998600276, 11.44779298504227860 ) ) ;
#99006=CARTESIAN_POINT ( 'NONE',  ( -112.6228709571500559, -29.50248528299804818, 1.056150453629043584 ) ) ;
#99007=CARTESIAN_POINT ( 'NONE',  ( -5.125883829288005344, 21.89707322345674712, -1.500000000000002220 ) ) ;
#99008=CARTESIAN_POINT ( 'NONE',  ( -111.9725711586931283, -25.11552134530501590, 2.805129186380271644 ) ) ;
#99009=VERTEX_POINT ( 'NONE', #1514 ) ;
#99010=CARTESIAN_POINT ( 'NONE',  ( -100.4498239493576648, -25.04307398257883932, 7.563174194274490780 ) ) ;
#99011=CARTESIAN_POINT ( 'NONE',  ( -12.94911239430987315, -14.73082512860577609, 11.49999999999999645 ) ) ;
#99012=CARTESIAN_POINT ( 'NONE',  ( -95.52287095715011844, -23.48783264082477373, -1.443836473390086139 ) ) ;
#99013=EDGE_CURVE ( 'NONE', #24726, #17192, #31952, .T. ) ;
#99014=DIRECTION ( 'NONE',  ( -3.773278334453080206E-23, 0.9999999999976377785, 2.173523156925979975E-06 ) ) ;
#99015=B_SPLINE_CURVE_WITH_KNOTS ( 'NONE', 3,
 ( #76339, #92566, #60652, #14445, #99666, #15444, #99181, #91079 ),
 .UNSPECIFIED., .F., .F.,
 ( 4, 2, 2, 4 ),
 ( -0.001224873891641429548, -0.0002244903592271130493, 0.0007758931731872034492, 0.002776660238015839915 ),
 .UNSPECIFIED. ) ;
#99016=VERTEX_POINT ( 'NONE', #48188 ) ;
#99017=CARTESIAN_POINT ( 'NONE',  ( -88.62596114253774715, -24.51419770103157703, 9.386484678747176957 ) ) ;
#99018=CARTESIAN_POINT ( 'NONE',  ( -36.52287095715006870, -23.47596703998600631, 11.44779298504229281 ) ) ;
#99019=CARTESIAN_POINT ( 'NONE',  ( -100.6373084487711225, -25.31439533618487303, 5.200261023079458589 ) ) ;
#99020=CARTESIAN_POINT ( 'NONE',  ( -42.55620429048339304, -23.48783264082477729, -1.443836473390073705 ) ) ;
#99021=CARTESIAN_POINT ( 'NONE',  ( -9.297559507673007317, 17.40068379117045083, 11.49999999999998934 ) ) ;
#99022=ORIENTED_EDGE ( 'NONE', *, *, #93348, .F. ) ;
#99025=DIRECTION ( 'NONE',  ( 0.000000000000000000, -2.173523156925979552E-06, 0.9999999999976378895 ) ) ;
#99028=ORIENTED_EDGE ( 'NONE', *, *, #49638, .F. ) ;
#99031=CARTESIAN_POINT ( 'NONE',  ( -55.58902656714176516, -24.52300882791528736, 0.6510814631126286001 ) ) ;
#99032=CARTESIAN_POINT ( 'NONE',  ( -118.5555942329009014, -23.96119346886881019, -0.6495511937832023630 ) ) ;
#99034=CARTESIAN_POINT ( 'NONE',  ( -70.15650799851037789, -25.24515045258689483, 5.327551117306890127 ) ) ;
#99036=CARTESIAN_POINT ( 'NONE',  ( -19.95764006394758638, 0.7380318605572177004, -1.500000000000002220 ) ) ;
#99038=B_SPLINE_CURVE_WITH_KNOTS ( 'NONE', 3,
 ( #48503, #63229, #55110, #79428 ),
 .UNSPECIFIED., .F., .F.,
 ( 4, 4 ),
 ( 0.6592456326193364413, 0.6602463796601018009 ),
 .UNSPECIFIED. ) ;
#99040=CARTESIAN_POINT ( 'NONE',  ( -45.63256516684009512, -24.73531770709095312, 8.716586749053515604 ) ) ;
#99041=ORIENTED_EDGE ( 'NONE', *, *, #41023, .F. ) ;
#99044=CARTESIAN_POINT ( 'NONE',  ( -80.59162667163354854, -24.40133493613050319, 9.663955038902802386 ) ) ;
#99045=CARTESIAN_POINT ( 'NONE',  ( -81.58953762381672448, -23.48783264082478794, -1.443836473390065711 ) ) ;
#99046=CARTESIAN_POINT ( 'NONE',  ( -39.58114864661853005, -24.51314013834315730, 0.6176544820404118452 ) ) ;
#99047=B_SPLINE_CURVE_WITH_KNOTS ( 'NONE', 3,
 ( #13700, #67512, #20812, #67025 ),
 .UNSPECIFIED., .F., .F.,
 ( 4, 4 ),
 ( 0.000000000000000000, 1.000000000000000000 ),
 .UNSPECIFIED. ) ;
#99049=CARTESIAN_POINT ( 'NONE',  ( -97.58953762381672448, -24.65952944569304961, 1.056160979905701902 ) ) ;
#99052=CARTESIAN_POINT ( 'NONE',  ( -111.5228709571500616, -29.50250786944525672, 11.44777988621622988 ) ) ;
#99054=CARTESIAN_POINT ( 'NONE',  ( -17.45352675615719917, 10.31968153043333380, -1.500000000000002220 ) ) ;
#99055=LINE ( 'NONE', #21928, #92220 ) ;
#99057=FACE_OUTER_BOUND ( 'NONE', #56203, .T. ) ;
#99061=B_SPLINE_CURVE_WITH_KNOTS ( 'NONE', 3,
 ( #76570, #14681, #37028, #59373, #37528, #68973 ),
 .UNSPECIFIED., .F., .F.,
 ( 4, 2, 4 ),
 ( 1.570887131794952276E-05, 0.001396322306279766060, 0.002776935741241582344 ),
 .UNSPECIFIED. ) ;
#99063=VECTOR ( 'NONE', #74697, 1000.000000000000114 ) ;
#99064=CARTESIAN_POINT ( 'NONE',  ( -19.68739882612603864, 4.164723872966736629, -1.500000000000002220 ) ) ;
#99065=CARTESIAN_POINT ( 'NONE',  ( 13.75562813033083742, -15.94169299924578453, 11.49999999999999645 ) ) ;
#99068=CARTESIAN_POINT ( 'NONE',  ( -22.03165466229905789, 1.424673820674137614, -1.500000000000002220 ) ) ;
#99069=EDGE_CURVE ( 'NONE', #93197, #74266, #60027, .T. ) ;
#99070=CARTESIAN_POINT ( 'NONE',  ( 20.13950599927006735, 4.067174238878714654, -1.500000000000002220 ) ) ;
#99071=PLANE ( 'NONE',  #25234 ) ;
#99074=VERTEX_POINT ( 'NONE', #41578 ) ;
#99075=DIRECTION ( 'NONE',  ( -3.773278334444166432E-23, 1.000000000000000000, 0.000000000000000000 ) ) ;
#99076=EDGE_LOOP ( 'NONE', ( #72197, #91734, #62062, #42977 ) ) ;
#99077=CARTESIAN_POINT ( 'NONE',  ( -99.40985337475474637, -25.19006306930774386, 3.256098372597241219 ) ) ;
#99078=LINE ( 'NONE', #38684, #68029 ) ;
#99082=CARTESIAN_POINT ( 'NONE',  ( -120.6228709571500417, -29.50250786944525672, 11.44777988621622811 ) ) ;
#99084=CARTESIAN_POINT ( 'NONE',  ( 19.39950376024442846, -7.079068461131618584, -1.500000000000002220 ) ) ;
#99085=CARTESIAN_POINT ( 'NONE',  ( -7.466173891270859286, -20.28576548065916541, 11.49999999999999645 ) ) ;
#99086=ORIENTED_EDGE ( 'NONE', *, *, #32601, .F. ) ;
#99087=LINE ( 'NONE', #58559, #79037 ) ;
#99089=CARTESIAN_POINT ( 'NONE',  ( -0.4079105510268487000, 22.33655531192813370, 11.49999999999998934 ) ) ;
#99090=B_SPLINE_CURVE_WITH_KNOTS ( 'NONE', 3,
 ( #13549, #36900, #30275, #68354 ),
 .UNSPECIFIED., .F., .F.,
 ( 4, 4 ),
 ( 0.000000000000000000, 9.999999999998897304E-05 ),
 .UNSPECIFIED. ) ;
#99091=CARTESIAN_POINT ( 'NONE',  ( -93.52287095715006160, -24.50216790748204687, 0.6166512839542578339 ) ) ;
#99092=CARTESIAN_POINT ( 'NONE',  ( -104.5562042904833930, -24.64898659630529210, 1.056161002820829919 ) ) ;
#99094=CARTESIAN_POINT ( 'NONE',  ( -43.52287095715007581, -23.47593901973090169, -1.443836447538997092 ) ) ;
#99095=CARTESIAN_POINT ( 'NONE',  ( -35.47207274640775410, -24.83644354573578639, 8.397322867130093016 ) ) ;
#99096=CARTESIAN_POINT ( 'NONE',  ( -15.12424899162716230, 14.39509690008720177, -1.500000000000002220 ) ) ;
#99097=VERTEX_POINT ( 'NONE', #73028 ) ;
#99098=EDGE_CURVE ( 'NONE', #40304, #67935, #11606, .T. ) ;
#99099=CARTESIAN_POINT ( 'NONE',  ( -86.63934676394221412, -23.73766607897671221, -1.055555164236432697 ) ) ;
#99100=ORIENTED_EDGE ( 'NONE', *, *, #86035, .F. ) ;
#99101=VERTEX_POINT ( 'NONE', #56813 ) ;
#99103=CARTESIAN_POINT ( 'NONE',  ( -109.5877440957333704, -24.51419770103157347, 9.386484678747171628 ) ) ;
#99104=CARTESIAN_POINT ( 'NONE',  ( 17.61891135320703938, 11.69080507458975227, -1.500000000000002220 ) ) ;
#99105=ORIENTED_EDGE ( 'NONE', *, *, #36422, .T. ) ;
#99106=CARTESIAN_POINT ( 'NONE',  ( -117.5936837924626701, -23.48783264082477018, -1.443836473390081254 ) ) ;
#99107=LINE ( 'NONE', #79154, #90376 ) ;
#99108=CARTESIAN_POINT ( 'NONE',  ( 21.36706796925463792, 4.321743776461201669, 11.49999999999998934 ) ) ;
#99109=CARTESIAN_POINT ( 'NONE',  ( -114.2228709571500644, -23.47596703998600276, 11.44779298504227683 ) ) ;
#99110=B_SPLINE_CURVE_WITH_KNOTS ( 'NONE', 3,
 ( #76723, #38171, #59042, #92958, #10117, #32965 ),
 .UNSPECIFIED., .F., .F.,
 ( 4, 2, 4 ),
 ( 3.122786320239759279E-05, 0.002624795872137489043, 0.005218363881072580514 ),
 .UNSPECIFIED. ) ;
#99111=CARTESIAN_POINT ( 'NONE',  ( -41.52287095715006870, -24.50216790748205042, 0.6166512839542425128 ) ) ;
#99113=CARTESIAN_POINT ( 'NONE',  ( -8.443908442993951269, 20.02826104456839218, -1.500000000000002220 ) ) ;
#99114=CARTESIAN_POINT ( 'NONE',  ( -71.27229073968156570, -25.24674082005258313, 4.988759856649874536 ) ) ;
#99115=CARTESIAN_POINT ( 'NONE',  ( -20.85237562250380350, -7.973873963886685345, 11.49999999999999645 ) ) ;
#99117=CARTESIAN_POINT ( 'NONE',  ( -57.52287095715003318, -23.73934037231757088, 11.05740245334328797 ) ) ;
#99120=VERTEX_POINT ( 'NONE', #97351 ) ;
#99123=ORIENTED_EDGE ( 'NONE', *, *, #74997, .F. ) ;
#99124=EDGE_CURVE ( 'NONE', #69709, #19646, #80691, .T. ) ;
#99125=CARTESIAN_POINT ( 'NONE',  ( -85.62287095715005592, -23.48786465467241413, 11.44779295918254114 ) ) ;
#99126=CARTESIAN_POINT ( 'NONE',  ( -10.79823215447539653, -18.26288818932900071, -1.500000000000002220 ) ) ;
#99129=CARTESIAN_POINT ( 'NONE',  ( -79.46053308078880661, -25.03138219016592103, 7.192627279560748654 ) ) ;
#99130=CARTESIAN_POINT ( 'NONE',  ( -59.52287095715004739, -24.66019654487199375, 8.947790411086128159 ) ) ;
#99132=CARTESIAN_POINT ( 'NONE',  ( -2.960655606634402748, -19.13016773636607581, 11.49999999999998934 ) ) ;
#99133=CARTESIAN_POINT ( 'NONE',  ( -31.52287095715006870, -24.35013146730202394, 9.818937971375110152 ) ) ;
#99135=CARTESIAN_POINT ( 'NONE',  ( 18.36381783059253081, 6.383776564742674964, 11.49999999999999645 ) ) ;
#99136=DIRECTION ( 'NONE',  ( -4.522247983293619802E-39, -2.173523156893721996E-06, 0.9999999999976377785 ) ) ;
#99138=EDGE_LOOP ( 'NONE', ( #1300, #42225, #68814, #97558 ) ) ;
#99141=CARTESIAN_POINT ( 'NONE',  ( -64.92287095715006728, -23.47596703998600631, 11.44779298504227860 ) ) ;
#99144=CARTESIAN_POINT ( 'NONE',  ( 10.60981200654714307, 16.52409317135366607, 11.49999999999998934 ) ) ;
#99148=CARTESIAN_POINT ( 'NONE',  ( -4.138935798035190849, -21.16376344109877294, 11.49999999999998934 ) ) ;
#99149=CARTESIAN_POINT ( 'NONE',  ( -33.48940092244485101, -24.35071581493542325, 9.817618358456039473 ) ) ;
#99150=CARTESIAN_POINT ( 'NONE',  ( -96.62287095715005592, -23.48783264082478794, -1.443836473390061936 ) ) ;
#99151=CARTESIAN_POINT ( 'NONE',  ( -81.62287095715005592, -24.64965695001468404, 8.947790433994182280 ) ) ;
#99152=CARTESIAN_POINT ( 'NONE',  ( -99.67151487672813914, -25.27473290596300615, 3.611381105655242063 ) ) ;
#99153=CARTESIAN_POINT ( 'NONE',  ( 15.83906049732654608, 16.74391201645830662, -1.500000000000002220 ) ) ;
#99154=EDGE_CURVE ( 'NONE', #16993, #90405, #42083, .T. ) ;
#99157=CARTESIAN_POINT ( 'NONE',  ( -93.63081067970922788, -24.15543982623907482, -0.2315651400026620677 ) ) ;
#99158=CARTESIAN_POINT ( 'NONE',  ( -50.70307649397453531, -25.30285855287542773, 4.744951912546983230 ) ) ;
#99159=CARTESIAN_POINT ( 'NONE',  ( 19.84801528777503776, 3.447069022702595742, 11.49999999999999645 ) ) ;
#99160=CARTESIAN_POINT ( 'NONE',  ( -45.62287095715004881, -24.99156045073392463, 7.747789690856161648 ) ) ;
#99161=CARTESIAN_POINT ( 'NONE',  ( -91.52287095715003318, -23.48783264082477018, -1.443836473390089248 ) ) ;
#99163=DIRECTION ( 'NONE',  ( 0.000000000000000000, 0.9999999999976377785, 2.173523156925979975E-06 ) ) ;
#99165=CARTESIAN_POINT ( 'NONE',  ( 17.57725459251073019, -9.329341740261039462, -1.500000000000002220 ) ) ;
#99167=CARTESIAN_POINT ( 'NONE',  ( -97.58953762381672448, -23.48786465467241058, 11.44779295918254114 ) ) ;
#99168=CARTESIAN_POINT ( 'NONE',  ( 9.697495225759652726, 17.24774500829319734, -1.500000000000002220 ) ) ;
#99169=FACE_OUTER_BOUND ( 'NONE', #37538, .T. ) ;
#99170=ADVANCED_FACE ( 'NONE', ( #80125 ), #3514, .T. ) ;
#99173=CARTESIAN_POINT ( 'NONE',  ( 11.79242832063081892, -16.95861370568002613, 11.49999999999999645 ) ) ;
#99174=CARTESIAN_POINT ( 'NONE',  ( -56.58953762381672448, -23.47593901973091235, -1.443836447539007972 ) ) ;
#99175=DIRECTION ( 'NONE',  ( -3.773278334453079030E-23, 0.9999999999976377785, 2.173523156925979128E-06 ) ) ;
#99176=DIRECTION ( 'NONE',  ( 0.000000000000000000, -2.173523156925980399E-06, 0.9999999999976378895 ) ) ;
#99177=CARTESIAN_POINT ( 'NONE',  ( 12.23086119556625206, 19.17791753167082192, 11.49999999999999645 ) ) ;
#99180=B_SPLINE_SURFACE_WITH_KNOTS ( 'NONE', 3, 3, ( 
 ( #95560, #42787, #73719, #19430 ),
 ( #33153, #18434, #4214, #26042 ),
 ( #57016, #96553, #34667, #11326 ),
 ( #64138, #35168, #86940, #88454 ),
 ( #26555, #10321, #95058, #49905 ),
 ( #17937, #80839, #65139, #48391 ),
 ( #42303, #71731, #56515, #50395 ) ),
 .UNSPECIFIED., .F., .F., .F.,
 ( 4, 3, 4 ),
 ( 4, 4 ),
 ( 0.3495694201722119865, 0.5199403837404874551, 0.6903113473087629792 ),
 ( 0.4867129260185943385, 0.5164839350294436748 ),
 .UNSPECIFIED. ) ;
#99181=CARTESIAN_POINT ( 'NONE',  ( -60.62287095715002039, -23.85196035786901803, -0.8779234886474974742 ) ) ;
#99183=CARTESIAN_POINT ( 'NONE',  ( -20.08517628505838815, -1.856936949192496300, 11.49999999999998934 ) ) ;
#99185=CARTESIAN_POINT ( 'NONE',  ( -41.45979626101074444, -25.28633313991813480, 4.315766560440735589 ) ) ;
#99187=ORIENTED_EDGE ( 'NONE', *, *, #3732, .F. ) ;
#99190=CARTESIAN_POINT ( 'NONE',  ( 22.67525425759127344, 3.225002893152739247, 11.49999999999998934 ) ) ;
#99191=CARTESIAN_POINT ( 'NONE',  ( -49.62287095715005592, -29.50247984919015209, -1.443849546365058689 ) ) ;
#99192=CARTESIAN_POINT ( 'NONE',  ( 16.53012286974688294, -13.99140274789385252, -1.500000000000002220 ) ) ;
#99193=DIRECTION ( 'NONE',  ( -3.773278334444167608E-23, 1.000000000000000000, 0.000000000000000000 ) ) ;
#99194=CARTESIAN_POINT ( 'NONE',  ( -114.6228709571500559, -24.64898659630528854, 1.056161002820831474 ) ) ;
#99196=CARTESIAN_POINT ( 'NONE',  ( -5.518977837361389582, -20.17201009624758257, 11.49999999999999645 ) ) ;
#99198=CARTESIAN_POINT ( 'NONE',  ( -27.83139521413862028, -24.79471210469401043, 2.282574248019634933 ) ) ;
#99200=CARTESIAN_POINT ( 'NONE',  ( -1.351711525931510449, 21.94731587555429186, 11.49999999999998934 ) ) ;
#99201=CARTESIAN_POINT ( 'NONE',  ( -105.5477487753952488, -24.83644354573579349, 8.397322867130096569 ) ) ;
#99202=CARTESIAN_POINT ( 'NONE',  ( -41.46538131673724337, -25.29087121120879544, 3.231378520143959765 ) ) ;
#99203=ADVANCED_FACE ( 'NONE', ( #27344 ), #57805, .F. ) ;
#99208=CARTESIAN_POINT ( 'NONE',  ( -72.51140272759705852, -23.96169478059712787, 10.65365249895718414 ) ) ;
#99210=ORIENTED_EDGE ( 'NONE', *, *, #27558, .F. ) ;
#99211=CARTESIAN_POINT ( 'NONE',  ( -59.55620429048340725, -23.47593901973091235, -1.443836447539007972 ) ) ;
#99212=CARTESIAN_POINT ( 'NONE',  ( -117.5895376238167103, -24.64965694238408034, 8.947790433994645909 ) ) ;
#99213=CARTESIAN_POINT ( 'NONE',  ( -36.55286501431240254, -23.96119346886880308, -0.6495511937832127991 ) ) ;
#99214=CARTESIAN_POINT ( 'NONE',  ( -10.82153711268468932, 17.32902648900640230, -1.500000000000002220 ) ) ;
#99215=EDGE_LOOP ( 'NONE', ( #57222, #15726, #11470, #37220 ) ) ;
#99217=CARTESIAN_POINT ( 'NONE',  ( -30.59367615247571237, -24.87212640336024805, 1.420893871182736579 ) ) ;
#99218=AXIS2_PLACEMENT_3D ( 'NONE', #41894, #72839, #39874 ) ;
#99220=CARTESIAN_POINT ( 'NONE',  ( -28.62287095715004881, -24.49675894734168580, 8.947790415257339092 ) ) ;
#99221=ORIENTED_EDGE ( 'NONE', *, *, #30452, .F. ) ;
#99223=CARTESIAN_POINT ( 'NONE',  ( -29.81002072791678614, -24.63645409607815395, 5.237832512065683233 ) ) ;
#99225=CARTESIAN_POINT ( 'NONE',  ( 7.312689604342500260, -19.48077458720139532, -1.500000000000002220 ) ) ;
#99226=ORIENTED_EDGE ( 'NONE', *, *, #87757, .F. ) ;
#99228=ORIENTED_EDGE ( 'NONE', *, *, #99013, .T. ) ;
#99229=EDGE_CURVE ( 'NONE', #40606, #31854, #73520, .T. ) ;
#99231=CARTESIAN_POINT ( 'NONE',  ( -28.62287095715004881, -23.31957264754183967, 11.44779298504227860 ) ) ;
#99232=EDGE_LOOP ( 'NONE', ( #2011, #43234, #20137, #59981 ) ) ;
#99235=CARTESIAN_POINT ( 'NONE',  ( -55.62287095715004881, -24.62285846362214770, 9.038163152653524435 ) ) ;
#99237=AXIS2_PLACEMENT_3D ( 'NONE', #25251, #57722, #65353 ) ;
#99238=FACE_OUTER_BOUND ( 'NONE', #79869, .T. ) ;
#99239=CARTESIAN_POINT ( 'NONE',  ( -91.58953762381672448, -23.47593901973091235, -1.443836447539002865 ) ) ;
#99241=CARTESIAN_POINT ( 'NONE',  ( 7.527104757430762128, -20.84474501729809859, 11.49999999999999645 ) ) ;
#99243=B_SPLINE_CURVE_WITH_KNOTS ( 'NONE', 3,
 ( #2328, #33257, #94659, #47998 ),
 .UNSPECIFIED., .F., .F.,
 ( 4, 4 ),
 ( 0.000000000000000000, 0.0001000000000000028644 ),
 .UNSPECIFIED. ) ;
#99244=DIRECTION ( 'NONE',  ( -3.773278334453080206E-23, 0.9999999999976377785, 2.173523156925979975E-06 ) ) ;
#99245=CARTESIAN_POINT ( 'NONE',  ( 5.572475817582897228, 21.94689365879375131, 11.49999999999998934 ) ) ;
#99246=EDGE_CURVE ( 'NONE', #64205, #56116, #89241, .T. ) ;
#99247=ADVANCED_FACE ( 'NONE', ( #21211 ), #13685, .T. ) ;
#99248=EDGE_CURVE ( 'NONE', #14217, #7016, #83109, .T. ) ;
#99249=CARTESIAN_POINT ( 'NONE',  ( -92.52287095715006160, -23.48783264083452593, -1.443836473374927820 ) ) ;
#99250=VERTEX_POINT ( 'NONE', #59291 ) ;
#99253=CARTESIAN_POINT ( 'NONE',  ( -80.77089339228673737, -25.31559268691879794, 4.999327289942788966 ) ) ;
#99254=B_SPLINE_CURVE_WITH_KNOTS ( 'NONE', 3,
 ( #70604, #53885, #84817, #31533, #63011, #16812 ),
 .UNSPECIFIED., .F., .F.,
 ( 4, 2, 4 ),
 ( 0.000000000000000000, 0.001380764517853249468, 0.002761529035706498936 ),
 .UNSPECIFIED. ) ;
#99256=CARTESIAN_POINT ( 'NONE',  ( 1.915021276000606454, 20.04344799065331628, -1.500000000000002220 ) ) ;
#99257=CARTESIAN_POINT ( 'NONE',  ( -78.62287095715005592, -24.50321055353805022, 9.387540953477522265 ) ) ;
#99258=ORIENTED_EDGE ( 'NONE', *, *, #20821, .T. ) ;
#99259=CARTESIAN_POINT ( 'NONE',  ( -94.52287095715006160, -29.50247984919015209, -1.443849546365051806 ) ) ;
#99260=CARTESIAN_POINT ( 'NONE',  ( 3.885606641962014329, -21.97303888676646721, -1.500000000000002220 ) ) ;
#99261=ADVANCED_FACE ( 'NONE', ( #82617 ), #44064, .T. ) ;
#99264=ORIENTED_EDGE ( 'NONE', *, *, #30405, .F. ) ;
#99265=CARTESIAN_POINT ( 'NONE',  ( -101.5468792378191978, -25.16257303515140009, 6.236250857614320076 ) ) ;
#99266=CARTESIAN_POINT ( 'NONE',  ( -119.6228709571500701, -23.48786465467241769, 11.44779295918253759 ) ) ;
#99267=LINE ( 'NONE', #29765, #76542 ) ;
#99270=CARTESIAN_POINT ( 'NONE',  ( 0.4223197742854877812, 19.52780805513575402, 11.49999999999998934 ) ) ;
#99272=DIRECTION ( 'NONE',  ( 0.000000000000000000, 2.173523156925980399E-06, -0.9999999999976378895 ) ) ;
#99273=CARTESIAN_POINT ( 'NONE',  ( -7.042111407433782055, -20.27750348750624099, 11.49999999999998934 ) ) ;
#99274=CARTESIAN_POINT ( 'NONE',  ( -25.53440485667337612, -24.92775324654290969, 4.657482463092957659 ) ) ;
#99277=CARTESIAN_POINT ( 'NONE',  ( 21.14566350062385780, -8.679158401671109857, -1.500000000000002220 ) ) ;
#99278=EDGE_CURVE ( 'NONE', #25716, #6738, #62530, .T. ) ;
#99280=CARTESIAN_POINT ( 'NONE',  ( -39.52287095715009002, -24.33832256527049154, 0.1851278514138551823 ) ) ;
#99281=CARTESIAN_POINT ( 'NONE',  ( -29.58953762381674579, -24.57075707507987161, 1.056161308047962377 ) ) ;
#99282=CARTESIAN_POINT ( 'NONE',  ( 18.80801646011137507, -6.797914457553222434, 11.49999999999999645 ) ) ;
#99284=CARTESIAN_POINT ( 'NONE',  ( -123.6228709571500417, -24.33832256526968862, 0.1851278514119932828 ) ) ;
#99285=DIRECTION ( 'NONE',  ( 0.000000000000000000, 0.9999999999976377785, 2.173523156925979975E-06 ) ) ;
#99287=PLANE ( 'NONE',  #42894 ) ;
#99288=CARTESIAN_POINT ( 'NONE',  ( -65.52287095715006160, -23.85229601348996553, 10.88205029486209341 ) ) ;
#99289=EDGE_CURVE ( 'NONE', #21767, #61568, #55178, .T. ) ;
#99290=CARTESIAN_POINT ( 'NONE',  ( 2.995010171738120786, 21.53247193037183038, -1.500000000000002220 ) ) ;
#99291=CARTESIAN_POINT ( 'NONE',  ( -60.55620429048339304, -25.00158670708908915, 2.256160236439166855 ) ) ;
#99292=CARTESIAN_POINT ( 'NONE',  ( 19.52168601723349894, 1.684101417132040979, -1.500000000000002220 ) ) ;
#99293=CARTESIAN_POINT ( 'NONE',  ( -34.52287095715006160, -24.65952944569303895, 1.056160979905690134 ) ) ;
#99294=ADVANCED_FACE ( 'NONE', ( #75994 ), #43659, .T. ) ;
#99295=VECTOR ( 'NONE', #95940, 1000.000000000000114 ) ;
#99297=ORIENTED_EDGE ( 'NONE', *, *, #80237, .T. ) ;
#99302=CARTESIAN_POINT ( 'NONE',  ( 12.01435098137705637, -16.61664908515649941, 11.49999999999999645 ) ) ;
#99303=CARTESIAN_POINT ( 'NONE',  ( -56.52287095715008292, -24.66019654487199375, 8.947790411086122830 ) ) ;
#99306=ADVANCED_FACE ( 'NONE', ( #48071 ), #100317, .F. ) ;
#99307=ORIENTED_EDGE ( 'NONE', *, *, #4434, .F. ) ;
#99310=CARTESIAN_POINT ( 'NONE',  ( -116.5939909856900982, -23.48786465467241769, 11.44779295918253759 ) ) ;
#99311=DIRECTION ( 'NONE',  ( -3.773278334453079618E-23, 0.9999999999976377785, 2.173523156925979975E-06 ) ) ;
#99313=CARTESIAN_POINT ( 'NONE',  ( 21.10734164270438029, -9.282589649079691085, 11.49999999999999645 ) ) ;
#99314=CARTESIAN_POINT ( 'NONE',  ( 17.57702471007113232, 14.52005670271990034, 11.49999999999998934 ) ) ;
#99315=CARTESIAN_POINT ( 'NONE',  ( -110.5904850311403180, -24.40133493613049964, 9.663955038902800609 ) ) ;
#99316=B_SPLINE_SURFACE_WITH_KNOTS ( 'NONE', 3, 3, ( 
 ( #63869, #26276, #17662, #57252 ),
 ( #10547, #26777, #48634, #65866 ),
 ( #18654, #72462, #80559, #81063 ),
 ( #10049, #95785, #42018, #71966 ),
 ( #72962, #11543, #88682, #42517 ),
 ( #95291, #25775, #2955, #34391 ),
 ( #65368, #3949, #96785, #58237 ) ),
 .UNSPECIFIED., .F., .F., .F.,
 ( 4, 3, 4 ),
 ( 4, 4 ),
 ( 0.7945040050992241421, 0.8970133687736505657, 0.9995227324480768782 ),
 ( 0.9397327963690478292, 0.9411793639427116220 ),
 .UNSPECIFIED. ) ;
#99319=DIRECTION ( 'NONE',  ( -3.773278334453080206E-23, 0.9999999999976377785, 2.173523156925979975E-06 ) ) ;
#99320=CARTESIAN_POINT ( 'NONE',  ( -103.9228709571500531, -23.47596703998600631, 11.44779298504227860 ) ) ;
#99321=CARTESIAN_POINT ( 'NONE',  ( 15.24057855588860377, 15.72025634131890470, -1.500000000000002220 ) ) ;
#99323=CARTESIAN_POINT ( 'NONE',  ( -87.50251410887271675, -24.66019654487200441, 8.947790411086112172 ) ) ;
#99325=DIRECTION ( 'NONE',  ( -3.773278334453079618E-23, 0.9999999999976377785, 2.173523156925979975E-06 ) ) ;
#99327=CARTESIAN_POINT ( 'NONE',  ( -107.6228709571500701, -23.47596703998600631, 11.44779298504227860 ) ) ;
#99328=ORIENTED_EDGE ( 'NONE', *, *, #42788, .T. ) ;
#99329=CARTESIAN_POINT ( 'NONE',  ( -7.302954156136775232, -19.11528491071161540, -1.500000000000002220 ) ) ;
#99330=EDGE_LOOP ( 'NONE', ( #72527, #2482, #29927, #20338 ) ) ;
#99331=VERTEX_POINT ( 'NONE', #30834 ) ;
#99334=CARTESIAN_POINT ( 'NONE',  ( 21.10734164270438029, -9.282589649079691085, 11.49999999999998934 ) ) ;
#99335=CARTESIAN_POINT ( 'NONE',  ( -61.60404008566307965, -23.73766607897669800, -1.055555164236459120 ) ) ;
#99336=CARTESIAN_POINT ( 'NONE',  ( 16.63042848490962555, -11.55671354112608817, -1.500000000000002220 ) ) ;
#99338=VERTEX_POINT ( 'NONE', #93223 ) ;
#99339=CARTESIAN_POINT ( 'NONE',  ( -27.14488594699098201, -24.92687995790785038, 3.118813907533751983 ) ) ;
#99340=CARTESIAN_POINT ( 'NONE',  ( -41.86252025446345471, -25.30041590689949160, 4.388877412580752591 ) ) ;
#99341=CARTESIAN_POINT ( 'NONE',  ( -128.5228709571500758, -23.47596703998600631, 11.44779298504227683 ) ) ;
#99342=CARTESIAN_POINT ( 'NONE',  ( -99.62961828089473215, -24.15620529776628445, 10.23563542870660115 ) ) ;
#99343=CARTESIAN_POINT ( 'NONE',  ( 5.397486108853063236, 20.74927772461418485, 11.49999999999999645 ) ) ;
#99345=PLANE ( 'NONE',  #69475 ) ;
#99346=FACE_OUTER_BOUND ( 'NONE', #27380, .T. ) ;
#99348=ORIENTED_EDGE ( 'NONE', *, *, #724, .F. ) ;
#99349=CARTESIAN_POINT ( 'NONE',  ( -13.38394104848841693, -15.81244124602197765, 11.49999999999998934 ) ) ;
#99351=EDGE_LOOP ( 'NONE', ( #77126, #83011, #17274, #43706 ) ) ;
#99352=EDGE_CURVE ( 'NONE', #61563, #30238, #43136, .T. ) ;
#99353=LINE ( 'NONE', #30348, #87513 ) ;
#99354=ORIENTED_EDGE ( 'NONE', *, *, #30978, .T. ) ;
#99357=EDGE_LOOP ( 'NONE', ( #9535, #74552, #91143, #45817 ) ) ;
#99358=EDGE_CURVE ( 'NONE', #19622, #37096, #84266, .T. ) ;
#99359=CARTESIAN_POINT ( 'NONE',  ( 16.22650188657148362, -14.79325693486936188, 11.49999999999999645 ) ) ;
#99360=EDGE_CURVE ( 'NONE', #50678, #66840, #51582, .T. ) ;
#99361=CARTESIAN_POINT ( 'NONE',  ( -37.66610885914807483, -23.48786465467240703, 11.44779295918255180 ) ) ;
#99362=CARTESIAN_POINT ( 'NONE',  ( 1.861690257272737847, 22.46465895387273903, 11.49999999999998934 ) ) ;
#99363=ADVANCED_FACE ( 'NONE', ( #84617 ), #63815, .F. ) ;
#99364=CARTESIAN_POINT ( 'NONE',  ( 4.154569570224219355, 20.57273982587956240, 11.49999999999998934 ) ) ;
#99365=FACE_OUTER_BOUND ( 'NONE', #59606, .T. ) ;
#99366=EDGE_CURVE ( 'NONE', #53195, #58571, #1894, .T. ) ;
#99367=AXIS2_PLACEMENT_3D ( 'NONE', #72497, #65901, #10581 ) ;
#99371=ORIENTED_EDGE ( 'NONE', *, *, #27384, .T. ) ;
#99372=CARTESIAN_POINT ( 'NONE',  ( -128.6228709571500417, -24.66019654487200441, 8.947790411086121054 ) ) ;
#99373=CARTESIAN_POINT ( 'NONE',  ( -20.49900048275977227, -6.559984590058941301, -1.500000000000002220 ) ) ;
#99375=CARTESIAN_POINT ( 'NONE',  ( -105.5228709571500900, -24.14406661686766142, 10.28769366194078216 ) ) ;
#99376=ORIENTED_EDGE ( 'NONE', *, *, #52896, .F. ) ;
#99377=CARTESIAN_POINT ( 'NONE',  ( -20.67868931609407213, -4.308284118179648736, 11.49999999999998934 ) ) ;
#99379=CARTESIAN_POINT ( 'NONE',  ( -64.59268794064412589, -24.15543982623906771, -0.2315651400026674800 ) ) ;
#99380=CARTESIAN_POINT ( 'NONE',  ( -130.5728709571500588, -23.47593901973090524, -1.443836447538995982 ) ) ;
#99382=CARTESIAN_POINT ( 'NONE',  ( -56.52287095715006870, -24.64965694238407323, 8.947790433994201820 ) ) ;
#99383=CARTESIAN_POINT ( 'NONE',  ( 13.49617185221842952, 17.62045156095830123, -1.500000000000002220 ) ) ;
#99385=CARTESIAN_POINT ( 'NONE',  ( -81.51736153681817143, -23.73791477778911840, 11.05961554403170943 ) ) ;
#99386=B_SPLINE_CURVE_WITH_KNOTS ( 'NONE', 3,
 ( #74978, #98820, #98316, #13580, #37929, #44549, #100300, #38429 ),
 .UNSPECIFIED., .F., .F.,
 ( 4, 2, 2, 4 ),
 ( 6.391158118955161585E-06, 0.002007136338672919646, 0.003007508928949900393, 0.004007881519226880705 ),
 .UNSPECIFIED. ) ;
#99387=EDGE_CURVE ( 'NONE', #100167, #37824, #68466, .T. ) ;
#99388=VERTEX_POINT ( 'NONE', #50561 ) ;
#99391=CARTESIAN_POINT ( 'NONE',  ( -41.86995616089613748, -25.27955781699870741, 4.210709737955789400 ) ) ;
#99392=CARTESIAN_POINT ( 'NONE',  ( -100.5618440256851329, -23.48783264082477018, -1.443836473390090580 ) ) ;
#99393=EDGE_CURVE ( 'NONE', #44655, #61715, #35345, .T. ) ;
#99394=CARTESIAN_POINT ( 'NONE',  ( -11.39837868854680814, -15.77482985264681403, -1.500000000000002220 ) ) ;
#99395=CARTESIAN_POINT ( 'NONE',  ( 8.370372042246325250, 19.68514866842044242, -1.500000000000002220 ) ) ;
#99397=DIRECTION ( 'NONE',  ( 0.000000000000000000, -2.173523156925980399E-06, 0.9999999999976378895 ) ) ;
#99398=CARTESIAN_POINT ( 'NONE',  ( -72.52287095715010423, -23.72773821059536914, 11.05748984161097503 ) ) ;
#99400=CARTESIAN_POINT ( 'NONE',  ( 15.43685675143394498, -16.52047792065556564, -1.500000000000002220 ) ) ;
#99401=B_SPLINE_SURFACE_WITH_KNOTS ( 'NONE', 3, 3, ( 
 ( #31272, #55633, #95181, #24653 ),
 ( #77929, #39390, #54624, #17048 ),
 ( #79448, #48015, #85558, #70344 ),
 ( #12434, #49020, #79951, #20052 ),
 ( #10437, #74340, #57633, #96187 ),
 ( #97180, #28170, #50507, #11441 ),
 ( #65264, #42905, #95682, #43404 ) ),
 .UNSPECIFIED., .F., .F., .F.,
 ( 4, 3, 4 ),
 ( 4, 4 ),
 ( 0.0004766839783816290664, 0.1029713700210892202, 0.2054660560637968092 ),
 ( 0.7696897931818312832, 0.7710576511941856781 ),
 .UNSPECIFIED. ) ;
#99402=ORIENTED_EDGE ( 'NONE', *, *, #52288, .T. ) ;
#99403=CARTESIAN_POINT ( 'NONE',  ( -128.5228709571500758, -24.65952944569305316, 1.056160979905707675 ) ) ;
#99405=CARTESIAN_POINT ( 'NONE',  ( 9.171884637996585710, -17.55225146786146695, 11.49999999999999645 ) ) ;
#99407=ORIENTED_EDGE ( 'NONE', *, *, #61396, .F. ) ;
#99408=CARTESIAN_POINT ( 'NONE',  ( -59.52287095715009002, -23.47593901973090524, -1.443836447538997092 ) ) ;
#99409=CARTESIAN_POINT ( 'NONE',  ( -80.62287095715005592, -29.50250786944525672, 11.44777988621623521 ) ) ;
#99410=CARTESIAN_POINT ( 'NONE',  ( 3.837509532605410278, -21.31939230324424628, 11.49999999999998934 ) ) ;
#99411=CARTESIAN_POINT ( 'NONE',  ( -27.16293832639682293, -24.78279603735616732, 7.495382070342732739 ) ) ;
#99412=CARTESIAN_POINT ( 'NONE',  ( 19.38287969867323213, 0.6573286442255052986, -1.500000000000002220 ) ) ;
#99414=CARTESIAN_POINT ( 'NONE',  ( -129.5228709571501042, -23.72773821059536914, 11.05748984161097503 ) ) ;
#99416=CARTESIAN_POINT ( 'NONE',  ( 1.944447714513537262, -19.71154682592685958, 11.49999999999998934 ) ) ;
#99417=ORIENTED_EDGE ( 'NONE', *, *, #100274, .F. ) ;
#99418=AXIS2_PLACEMENT_3D ( 'NONE', #81002, #19590, #66295 ) ;
#99419=CARTESIAN_POINT ( 'NONE',  ( 16.59675031405745571, -11.69241480613374407, 11.49999999999999645 ) ) ;
#99420=CARTESIAN_POINT ( 'NONE',  ( -80.64006940006906632, -24.15503026093913164, -0.2815557561904567518 ) ) ;
#99424=CARTESIAN_POINT ( 'NONE',  ( -102.5574997761123939, -23.73791477778911840, 11.05961554403170410 ) ) ;
#99426=CARTESIAN_POINT ( 'NONE',  ( -49.53270844027763786, -25.25214452993709813, 5.057855935191842178 ) ) ;
#99427=B_SPLINE_CURVE_WITH_KNOTS ( 'NONE', 3,
 ( #92559, #77326, #53527, #77820 ),
 .UNSPECIFIED., .F., .F.,
 ( 4, 4 ),
 ( 1.387778780781445521E-17, 9.999999999997510880E-05 ),
 .UNSPECIFIED. ) ;
#99428=CARTESIAN_POINT ( 'NONE',  ( -47.55620429048340014, -23.47593901973091235, -1.443836447539009749 ) ) ;
#99430=CARTESIAN_POINT ( 'NONE',  ( 4.397486433803790007, -19.56896378179033036, 11.49999999999998934 ) ) ;
#99434=CARTESIAN_POINT ( 'NONE',  ( 18.56524475492553705, -13.42312393814442650, 11.49999999999999645 ) ) ;
#99435=CARTESIAN_POINT ( 'NONE',  ( -102.5228709571500616, -23.72747288104470442, -1.053458166803225016 ) ) ;
#99436=FACE_OUTER_BOUND ( 'NONE', #19016, .T. ) ;
#99437=CARTESIAN_POINT ( 'NONE',  ( -59.62287095715003460, -23.72747288104441665, -1.053458166803663332 ) ) ;
#99438=DIRECTION ( 'NONE',  ( 3.773278334444167608E-23, -1.000000000000000000, 0.000000000000000000 ) ) ;
#99442=ORIENTED_EDGE ( 'NONE', *, *, #27688, .T. ) ;
#99443=CARTESIAN_POINT ( 'NONE',  ( -11.21218820807429140, -16.99972530465495169, -1.500000000000002220 ) ) ;
#99445=ORIENTED_EDGE ( 'NONE', *, *, #51790, .T. ) ;
#99446=CARTESIAN_POINT ( 'NONE',  ( 22.74528686061176685, 3.085755641335488964, 11.49999999999998934 ) ) ;
#99447=CARTESIAN_POINT ( 'NONE',  ( -115.5562042904833788, -23.48786465467242124, 11.44779295918253759 ) ) ;
#99449=CARTESIAN_POINT ( 'NONE',  ( -95.62287095715005592, -29.50248528299804818, 1.056150453629042030 ) ) ;
#99450=CARTESIAN_POINT ( 'NONE',  ( -67.52287095715006160, -24.64965694238407323, 8.947790433994200043 ) ) ;
#99451=CARTESIAN_POINT ( 'NONE',  ( -96.62287095715009855, -24.33832256526969928, 0.1851278514119889529 ) ) ;
#99452=CARTESIAN_POINT ( 'NONE',  ( -4.730540317195566224, 20.75322969461001676, 11.49999999999999645 ) ) ;
#99455=CARTESIAN_POINT ( 'NONE',  ( 8.998109643811913472, -20.30750954041392120, -1.500000000000002220 ) ) ;
#99456=CARTESIAN_POINT ( 'NONE',  ( -3.087264924507187924, 20.40197043678811539, 11.49999999999998934 ) ) ;
#99457=ORIENTED_EDGE ( 'NONE', *, *, #79417, .F. ) ;
#99458=ORIENTED_EDGE ( 'NONE', *, *, #56785, .F. ) ;
#99459=EDGE_CURVE ( 'NONE', #67442, #95555, #5559, .T. ) ;
#99460=CARTESIAN_POINT ( 'NONE',  ( -109.2582164645601779, -25.31627313540426627, 5.068133679678900272 ) ) ;
#99461=CARTESIAN_POINT ( 'NONE',  ( -55.22287095715006444, -23.47596703998600276, 11.44779298504227860 ) ) ;
#99462=ORIENTED_EDGE ( 'NONE', *, *, #31686, .F. ) ;
#99464=ORIENTED_EDGE ( 'NONE', *, *, #81631, .T. ) ;
#99466=CARTESIAN_POINT ( 'NONE',  ( -124.6228709571500559, -29.50250786944525672, 11.44777988621622811 ) ) ;
#99467=CARTESIAN_POINT ( 'NONE',  ( 19.25983760003161294, 7.974354923662064998, -1.500000000000002220 ) ) ;
#99468=CARTESIAN_POINT ( 'NONE',  ( 0.2638585030419089428, -21.76204025362994798, 11.49999999999999645 ) ) ;
#99469=VECTOR ( 'NONE', #66166, 1000.000000000000114 ) ;
#99470=EDGE_CURVE ( 'NONE', #42504, #37822, #83008, .T. ) ;
#99471=CARTESIAN_POINT ( 'NONE',  ( -51.61612386428029708, -25.12985818678743399, 7.066459036000934724 ) ) ;
#99473=CARTESIAN_POINT ( 'NONE',  ( -6.716530693746936898, -21.44081863256500142, -1.500000000000002220 ) ) ;
#99474=EDGE_CURVE ( 'NONE', #17843, #16362, #88133, .T. ) ;
#99475=CARTESIAN_POINT ( 'NONE',  ( -50.64790834543075704, -25.31296758314977779, 4.705120360976434490 ) ) ;
#99476=ORIENTED_EDGE ( 'NONE', *, *, #18024, .F. ) ;
#99477=CARTESIAN_POINT ( 'NONE',  ( -50.52287095715006160, -24.63345952396255001, 9.038047939301510070 ) ) ;
#99478=CARTESIAN_POINT ( 'NONE',  ( -57.52287095715005449, -24.65952944569304606, 1.056160979905695463 ) ) ;
#99480=ADVANCED_FACE ( 'NONE', ( #89128 ), #76907, .T. ) ;
#99481=EDGE_LOOP ( 'NONE', ( #93006, #94840, #82322, #48665 ) ) ;
#99482=ADVANCED_FACE ( 'NONE', ( #37827 ), #46154, .T. ) ;
#99484=FACE_OUTER_BOUND ( 'NONE', #75852, .T. ) ;
#99485=ORIENTED_EDGE ( 'NONE', *, *, #48715, .F. ) ;
#99486=CARTESIAN_POINT ( 'NONE',  ( -19.99249555334884221, 7.427959064407942513, -1.500000000000002220 ) ) ;
#99489=CARTESIAN_POINT ( 'NONE',  ( -19.58807393344005376, -7.628504261335002923, -1.500000000000002220 ) ) ;
#99490=CARTESIAN_POINT ( 'NONE',  ( -30.48115194396658012, -24.75308503270343152, 1.363670884829966123 ) ) ;
#99491=CARTESIAN_POINT ( 'NONE',  ( -41.46611000704998418, -25.28892616455412323, 4.188173659901108792 ) ) ;
#99493=CARTESIAN_POINT ( 'NONE',  ( 21.66556372666567754, 3.824538051775513647, -1.500000000000002220 ) ) ;
#99494=CARTESIAN_POINT ( 'NONE',  ( -87.51096306996832652, -24.15543982623908192, -0.2315651400026449980 ) ) ;
#99495=EDGE_LOOP ( 'NONE', ( #69019, #34133, #62800, #40101 ) ) ;
#99497=CARTESIAN_POINT ( 'NONE',  ( -84.54456340005228299, -24.51419770103157347, 9.386484678747175181 ) ) ;
#99499=CARTESIAN_POINT ( 'NONE',  ( -0.008164624327092516801, -22.94430252198347375, 6.147794833475636267 ) ) ;
#99500=CARTESIAN_POINT ( 'NONE',  ( 10.72677997844354536, -18.41129465587203740, 11.49999999999998934 ) ) ;
#99501=CARTESIAN_POINT ( 'NONE',  ( -98.59115901530434201, -24.15620529776628800, 10.23563542870660292 ) ) ;
#99503=CARTESIAN_POINT ( 'NONE',  ( -122.6228709571500559, -24.65952944569305316, 1.056160979905706343 ) ) ;
#99504=FACE_OUTER_BOUND ( 'NONE', #58742, .T. ) ;
#99505=CARTESIAN_POINT ( 'NONE',  ( -21.66288588771858770, -5.991481186202806342, -1.500000000000002220 ) ) ;
#99509=CARTESIAN_POINT ( 'NONE',  ( 19.59400933563812330, 0.1774559437341752532, 11.49999999999999645 ) ) ;
#99510=CARTESIAN_POINT ( 'NONE',  ( -125.6228709571500559, -24.83602698348162363, 1.605859176311269954 ) ) ;
#99511=CARTESIAN_POINT ( 'NONE',  ( -76.52287095715007581, -24.64965694238408034, 8.947790433994198267 ) ) ;
#99512=VERTEX_POINT ( 'NONE', #89623 ) ;
#99513=CARTESIAN_POINT ( 'NONE',  ( -69.45716761675758733, -25.30512913829650401, 5.118693047570955557 ) ) ;
#99514=CARTESIAN_POINT ( 'NONE',  ( -124.5120848053583131, -25.40067164642711361, 5.394116434732633358 ) ) ;
#99515=CARTESIAN_POINT ( 'NONE',  ( -124.5541588009910470, -24.66019654487200441, 8.947790411086108620 ) ) ;
#99517=CARTESIAN_POINT ( 'NONE',  ( -17.00503767097633556, -9.977476526402845991, -1.500000000000002220 ) ) ;
#99521=VECTOR ( 'NONE', #97811, 1000.000000000000114 ) ;
#99524=ORIENTED_EDGE ( 'NONE', *, *, #67091, .T. ) ;
#99527=CARTESIAN_POINT ( 'NONE',  ( -55.52866950233528343, -24.92564183028978775, 1.928384488918253092 ) ) ;
#99528=CARTESIAN_POINT ( 'NONE',  ( -99.33721417192995773, -25.03145088751183422, 7.148561016989910755 ) ) ;
#99532=CARTESIAN_POINT ( 'NONE',  ( -12.72357806474857966, 15.40231687525621318, 11.49999999999998934 ) ) ;
#99533=VECTOR ( 'NONE', #58796, 1000.000000000000114 ) ;
#99534=CARTESIAN_POINT ( 'NONE',  ( -32.50560601784287229, -24.86181184613565165, 1.747789954104514987 ) ) ;
#99535=CARTESIAN_POINT ( 'NONE',  ( -45.48403108558225227, -24.63419186844611630, 9.035850630976932862 ) ) ;
#99538=DIRECTION ( 'NONE',  ( -3.773278334453079030E-23, 0.9999999999976377785, 2.173523156925979128E-06 ) ) ;
#99541=CARTESIAN_POINT ( 'NONE',  ( -128.5228709571500758, -29.50248528299804818, 1.056150453629047137 ) ) ;
#99542=EDGE_CURVE ( 'NONE', #57842, #3242, #32146, .T. ) ;
#99544=CARTESIAN_POINT ( 'NONE',  ( -79.62287095715011276, -24.51387760970725083, 9.387446482453428942 ) ) ;
#99545=CARTESIAN_POINT ( 'NONE',  ( -112.6228709571500559, -24.64898659630368272, 1.056161002820831474 ) ) ;
#99546=ORIENTED_EDGE ( 'NONE', *, *, #5396, .T. ) ;
#99547=CARTESIAN_POINT ( 'NONE',  ( 0.7435384974594729801, 20.27106041150680937, 11.49999999999998934 ) ) ;
#99548=CARTESIAN_POINT ( 'NONE',  ( -76.62287095715007013, -23.47596703998600631, 11.44779298504227860 ) ) ;
#99550=B_SPLINE_CURVE_WITH_KNOTS ( 'NONE', 3,
 ( #69674, #45345, #23981, #54953, #84389, #16371, #61071, #30600 ),
 .UNSPECIFIED., .F., .F.,
 ( 4, 2, 2, 4 ),
 ( 0.000000000000000000, 0.002001079623178217588, 0.003001619434767328985, 0.004002159246356440381 ),
 .UNSPECIFIED. ) ;
#99552=ORIENTED_EDGE ( 'NONE', *, *, #70633, .T. ) ;
#99555=CARTESIAN_POINT ( 'NONE',  ( 6.436487395234643749, 19.08016507665710648, -1.500000000000002220 ) ) ;
#99556=CARTESIAN_POINT ( 'NONE',  ( 21.06685942672242362, 1.161445541649065882, 11.49999999999999645 ) ) ;
#99558=LINE ( 'NONE', #48192, #7691 ) ;
#99559=CARTESIAN_POINT ( 'NONE',  ( -11.88820881604258339, -18.65297325734525913, 11.49999999999998934 ) ) ;
#99560=CARTESIAN_POINT ( 'NONE',  ( -20.49763986188970932, -1.003951800832726615, -1.500000000000002220 ) ) ;
#99561=CARTESIAN_POINT ( 'NONE',  ( -41.62287095715006302, -24.65952944569303895, 1.056160979905692576 ) ) ;
#99562=CARTESIAN_POINT ( 'NONE',  ( -60.51214155151011198, -23.85016227208580375, -0.8807180028928355275 ) ) ;
#99564=DIRECTION ( 'NONE',  ( 0.000000000000000000, -0.9999999999976377785, -2.173523156925979975E-06 ) ) ;
#99566=CARTESIAN_POINT ( 'NONE',  ( -35.52287095715008292, -23.85229601348997264, 10.88205029486209696 ) ) ;
#99567=B_SPLINE_SURFACE_WITH_KNOTS ( 'NONE', 3, 3, ( 
 ( #15224, #20826, #44186, #60422 ),
 ( #37566, #21822, #52298, #60917 ),
 ( #91846, #28951, #52798, #29443 ),
 ( #53801, #51802, #76607, #38060 ),
 ( #30453, #83733, #36066, #75122 ),
 ( #44688, #14213, #6113, #61417 ),
 ( #67529, #84230, #5615, #67040 ) ),
 .UNSPECIFIED., .F., .F., .F.,
 ( 4, 3, 4 ),
 ( 4, 4 ),
 ( 0.7945040050992234759, 0.8970133687736497885, 0.9995227324480761011 ),
 ( 0.5296285832068964305, 0.5308858194615871939 ),
 .UNSPECIFIED. ) ;
#99568=CARTESIAN_POINT ( 'NONE',  ( -87.55620429048337883, -24.66019654487199730, 8.947790411086126383 ) ) ;
#99569=VERTEX_POINT ( 'NONE', #74393 ) ;
#99570=ORIENTED_EDGE ( 'NONE', *, *, #94608, .F. ) ;
#99572=DIRECTION ( 'NONE',  ( -3.773278334453079030E-23, 0.9999999999976377785, 2.173523156925979128E-06 ) ) ;
#99573=CARTESIAN_POINT ( 'NONE',  ( -40.62287095715005592, -23.48783264082478084, -1.443836473390072817 ) ) ;
#99574=CARTESIAN_POINT ( 'NONE',  ( -68.55932689068598052, -23.73791477778911840, 11.05961554403170943 ) ) ;
#99575=CARTESIAN_POINT ( 'NONE',  ( -20.25002411749221665, -3.895867502427604379, -1.500000000000002220 ) ) ;
#99576=CARTESIAN_POINT ( 'NONE',  ( -15.70146493180990888, -14.86199287721409590, 11.49999999999999645 ) ) ;
#99577=ORIENTED_EDGE ( 'NONE', *, *, #24926, .T. ) ;
#99579=CARTESIAN_POINT ( 'NONE',  ( -100.5228709571500616, -23.47596703998600631, 11.44779298504228215 ) ) ;
#99580=CARTESIAN_POINT ( 'NONE',  ( -60.62287095715007013, -24.82558206586144323, 1.605769216559442158 ) ) ;
#99581=CARTESIAN_POINT ( 'NONE',  ( -13.97600220251353953, -17.46790257487896270, -1.500000000000002220 ) ) ;
#99582=LINE ( 'NONE', #36219, #61055 ) ;
#99585=CARTESIAN_POINT ( 'NONE',  ( -100.5548270777744335, -25.31262531776226510, 4.733991798650357019 ) ) ;
#99587=ADVANCED_FACE ( 'NONE', ( #75379 ), #28259, .T. ) ;
#99588=CARTESIAN_POINT ( 'NONE',  ( -20.36979505965413395, -4.774807507659313721, -1.500000000000002220 ) ) ;
#99590=VERTEX_POINT ( 'NONE', #30202 ) ;
#99591=VECTOR ( 'NONE', #52783, 1000.000000000000227 ) ;
#99592=CARTESIAN_POINT ( 'NONE',  ( -67.55389080268135160, -23.96169478059713853, 10.65365249895717881 ) ) ;
#99593=EDGE_LOOP ( 'NONE', ( #80785, #53999, #69311, #75542 ) ) ;
#99595=CARTESIAN_POINT ( 'NONE',  ( -109.6276321201155923, -24.15620529776628800, 10.23563542870660115 ) ) ;
#99596=CARTESIAN_POINT ( 'NONE',  ( -21.01389645921736360, -2.595061309317715281, -1.500000000000002220 ) ) ;
#99597=VERTEX_POINT ( 'NONE', #69275 ) ;
#99598=CARTESIAN_POINT ( 'NONE',  ( -117.5924212553219661, -23.73766607897670511, -1.055555164236445798 ) ) ;
#99599=DIRECTION ( 'NONE',  ( 0.000000000000000000, -2.173523156925980399E-06, 0.9999999999976378895 ) ) ;
#99600=CARTESIAN_POINT ( 'NONE',  ( 1.472770742059883897, 21.73951962378590963, 11.49999999999998934 ) ) ;
#99601=DIRECTION ( 'NONE',  ( -1.000000000000000000, -3.773278334444167608E-23, -8.201307833595939069E-29 ) ) ;
#99602=CARTESIAN_POINT ( 'NONE',  ( -41.52287095715006160, -23.94994826722564696, -0.6494450866342750261 ) ) ;
#99603=CARTESIAN_POINT ( 'NONE',  ( -84.52287095715006160, -24.64965694238406613, 8.947790433994198267 ) ) ;
#99604=CARTESIAN_POINT ( 'NONE',  ( 21.72137571921558319, 1.130696696492564213, -1.500000000000002220 ) ) ;
#99605=CARTESIAN_POINT ( 'NONE',  ( -41.58953762381673158, -24.64898659630367561, 1.056161002820379391 ) ) ;
#99606=CARTESIAN_POINT ( 'NONE',  ( 15.82088602905085750, -15.72875506571707760, 11.49999999999999645 ) ) ;
#99607=ORIENTED_EDGE ( 'NONE', *, *, #70209, .F. ) ;
#99608=EDGE_CURVE ( 'NONE', #44325, #8909, #52642, .T. ) ;
#99610=CARTESIAN_POINT ( 'NONE',  ( -85.53959221982877636, -24.92592662359561473, 8.075495903018000021 ) ) ;
#99612=ORIENTED_EDGE ( 'NONE', *, *, #68946, .T. ) ;
#99614=VECTOR ( 'NONE', #62940, 1000.000000000000114 ) ;
#99616=EDGE_LOOP ( 'NONE', ( #16011, #32347, #2393, #50061 ) ) ;
#99617=CARTESIAN_POINT ( 'NONE',  ( -124.5562042904834215, -24.66019654487200441, 8.947790411086121054 ) ) ;
#99618=CARTESIAN_POINT ( 'NONE',  ( 18.56724428474754518, 10.22298014144217859, 11.49999999999998934 ) ) ;
#99620=CARTESIAN_POINT ( 'NONE',  ( -80.18401481691103072, -25.03138293780579460, 7.536603307588053191 ) ) ;
#99621=CARTESIAN_POINT ( 'NONE',  ( -59.55620429048338593, -24.66019654487199730, 8.947790411086135265 ) ) ;
#99622=DIRECTION ( 'NONE',  ( -3.773278334453080206E-23, 0.9999999999976377785, 2.173523156925979975E-06 ) ) ;
#99623=CARTESIAN_POINT ( 'NONE',  ( -5.843762028675351772, -18.45606589188993141, 11.49999999999998934 ) ) ;
#99625=EDGE_LOOP ( 'NONE', ( #51866, #37961, #78382, #76650 ) ) ;
#99626=CARTESIAN_POINT ( 'NONE',  ( -14.39514105012195344, 13.04300321504834947, 11.49999999999999645 ) ) ;
#99629=CARTESIAN_POINT ( 'NONE',  ( -78.52287095715006160, -23.47596703998600631, 11.44779298504228571 ) ) ;
#99633=CARTESIAN_POINT ( 'NONE',  ( 6.560884470684795744, 18.50665934316380756, -1.500000000000002220 ) ) ;
#99634=CARTESIAN_POINT ( 'NONE',  ( -41.34727404100192416, -25.27806037341403211, 4.610739018140001200 ) ) ;
#99637=CARTESIAN_POINT ( 'NONE',  ( 19.30674495121141376, 9.566621930910674365, 11.49999999999998934 ) ) ;
#99638=B_SPLINE_CURVE_WITH_KNOTS ( 'NONE', 3,
 ( #92969, #54427, #85360, #87369 ),
 .UNSPECIFIED., .F., .F.,
 ( 4, 4 ),
 ( 0.8604003152822103928, 0.8694067465543262596 ),
 .UNSPECIFIED. ) ;
#99639=CARTESIAN_POINT ( 'NONE',  ( -33.55275594712417586, -23.96169478059712432, 10.65365249895719124 ) ) ;
#99642=CARTESIAN_POINT ( 'NONE',  ( -20.21456430084473155, -11.12997698910670152, -1.500000000000002220 ) ) ;
#99643=EDGE_CURVE ( 'NONE', #72422, #29962, #19915, .T. ) ;
#99645=CARTESIAN_POINT ( 'NONE',  ( -74.55620429048340725, -23.47596703998600276, 11.44779298504227683 ) ) ;
#99646=LINE ( 'NONE', #14919, #18315 ) ;
#99647=CARTESIAN_POINT ( 'NONE',  ( -2.706554608146168217, 19.95013100808389339, 11.49999999999999645 ) ) ;
#99648=CARTESIAN_POINT ( 'NONE',  ( -126.5228709571499763, -23.48783264082477018, -1.443836473390082142 ) ) ;
#99650=CARTESIAN_POINT ( 'NONE',  ( -110.3346797185884327, -25.18492896333868813, 3.293943116708551777 ) ) ;
#99651=CARTESIAN_POINT ( 'NONE',  ( -28.62287095715004881, -29.50250786944455328, 11.44777956126000618 ) ) ;
#99652=CARTESIAN_POINT ( 'NONE',  ( -110.3346797185884327, -25.18425582661724249, 3.293943118171629880 ) ) ;
#99653=CARTESIAN_POINT ( 'NONE',  ( -4.768723929037996356, 19.30091236029735668, 11.49999999999998934 ) ) ;
#99655=CARTESIAN_POINT ( 'NONE',  ( 17.61170953066113398, -8.936083093766256980, -1.500000000000002220 ) ) ;
#99656=CARTESIAN_POINT ( 'NONE',  ( -56.54793356327564169, -24.15543982623907127, -0.2315651400026670359 ) ) ;
#99658=CARTESIAN_POINT ( 'NONE',  ( -39.04530173637052570, -25.29116805862484796, 4.154356755045506056 ) ) ;
#99659=CARTESIAN_POINT ( 'NONE',  ( -66.58953762381672448, -23.47593901973091235, -1.443836447539006196 ) ) ;
#99660=CARTESIAN_POINT ( 'NONE',  ( -20.51892249978613236, 2.527598752449112585, 11.49999999999999645 ) ) ;
#99661=CARTESIAN_POINT ( 'NONE',  ( -128.6228709571500417, -24.64965695001469115, 8.947790433994173398 ) ) ;
#99663=CARTESIAN_POINT ( 'NONE',  ( -35.62287095715005592, -23.47596703998600276, 11.44779298504227505 ) ) ;
#99664=CARTESIAN_POINT ( 'NONE',  ( 20.21490908150494192, 10.32750977814155391, 11.49999999999999645 ) ) ;
#99666=CARTESIAN_POINT ( 'NONE',  ( -60.62287095715003460, -24.52232992886363760, 0.6492154411906152500 ) ) ;
#99667=CARTESIAN_POINT ( 'NONE',  ( -69.37510736016693613, -25.21906335291104995, 6.451581876237428403 ) ) ;
#99668=CARTESIAN_POINT ( 'NONE',  ( 5.087728227403598424, 19.53446797131710611, -1.500000000000002220 ) ) ;
#99669=CARTESIAN_POINT ( 'NONE',  ( -63.64183085114759564, -23.96119346886879953, -0.6495511937832106897 ) ) ;
#99671=CARTESIAN_POINT ( 'NONE',  ( -52.52287095715005449, -24.33927499327855770, 9.819080762295818943 ) ) ;
#99672=EDGE_CURVE ( 'NONE', #27395, #29076, #72071, .T. ) ;
#99673=ORIENTED_EDGE ( 'NONE', *, *, #49923, .T. ) ;
#99676=LINE ( 'NONE', #46413, #93863 ) ;
#99677=CARTESIAN_POINT ( 'NONE',  ( 22.85676281555306844, 1.471244944367766649, 11.49999999999998934 ) ) ;
#99678=CARTESIAN_POINT ( 'NONE',  ( -50.75699389676201889, -25.27420573916653623, 3.343798433542797710 ) ) ;
#99679=CARTESIAN_POINT ( 'NONE',  ( 1.064956243273112557, 21.61254047163424019, -1.500000000000002220 ) ) ;
#99681=DIRECTION ( 'NONE',  ( 0.000000000000000000, -0.9999999999976377785, -2.173523156925979975E-06 ) ) ;
#99682=CARTESIAN_POINT ( 'NONE',  ( 0.8369575198195864374, -20.89415947959451003, 11.49999999999999645 ) ) ;
#99684=CARTESIAN_POINT ( 'NONE',  ( -68.94292010565295925, -25.31612680529077508, 6.048223976952783687 ) ) ;
#99685=CARTESIAN_POINT ( 'NONE',  ( -6.199593828526920092, 21.14725108817225419, -1.500000000000002220 ) ) ;
#99686=CARTESIAN_POINT ( 'NONE',  ( -105.5930580087945145, -24.15602025860896163, 10.28564288303535967 ) ) ;
#99687=CARTESIAN_POINT ( 'NONE',  ( -28.57615893954310238, -24.79700241673980088, 7.256892281947859402 ) ) ;
#99690=CARTESIAN_POINT ( 'NONE',  ( -90.54141365085332893, -24.92592662359561118, 8.075495903017998245 ) ) ;
#99692=PLANE ( 'NONE',  #85771 ) ;
#99695=ADVANCED_FACE ( 'NONE', ( #49957 ), #41842, .T. ) ;
#99696=CARTESIAN_POINT ( 'NONE',  ( -71.51121550292000961, -23.96169478059713498, 10.65365249895718058 ) ) ;
#99698=CARTESIAN_POINT ( 'NONE',  ( -36.49045368110912335, -24.34968618360933235, 0.1864209137778783110 ) ) ;
#99699=CARTESIAN_POINT ( 'NONE',  ( 19.18951349294833264, 7.196795126939715459, -1.500000000000002220 ) ) ;
#99702=CARTESIAN_POINT ( 'NONE',  ( -30.60993385648455956, -24.45056191361606679, 9.787827635114014768 ) ) ;
#99703=CARTESIAN_POINT ( 'NONE',  ( -89.81226385320383088, -25.22391155068715207, 6.409327647370969494 ) ) ;
#99704=CARTESIAN_POINT ( 'NONE',  ( 20.70802603420765564, 8.137917507125113303, -1.500000000000002220 ) ) ;
#99707=ORIENTED_EDGE ( 'NONE', *, *, #15754, .T. ) ;
#99709=CARTESIAN_POINT ( 'NONE',  ( -64.58953762381672448, -23.48786465467241413, 11.44779295918254824 ) ) ;
#99711=EDGE_CURVE ( 'NONE', #46308, #47247, #1784, .T. ) ;
#99712=CARTESIAN_POINT ( 'NONE',  ( 5.171613189315443115, 20.13430294385436881, 11.49999999999998934 ) ) ;
#99716=ORIENTED_EDGE ( 'NONE', *, *, #12202, .F. ) ;
#99717=B_SPLINE_CURVE_WITH_KNOTS ( 'NONE', 3,
 ( #7872, #84994, #79379, #15478 ),
 .UNSPECIFIED., .F., .F.,
 ( 4, 4 ),
 ( 0.000000000000000000, 0.0001000000000000028644 ),
 .UNSPECIFIED. ) ;
#99718=CARTESIAN_POINT ( 'NONE',  ( -98.52287095715010423, -24.35013146730204525, 9.818937971375097717 ) ) ;
#99725=CARTESIAN_POINT ( 'NONE',  ( -40.62287095715005592, -23.48786465467240347, 11.44779295918255180 ) ) ;
#99726=CARTESIAN_POINT ( 'NONE',  ( -109.0201204086170037, -25.24933767340982271, 3.731844282071034691 ) ) ;
#99728=CARTESIAN_POINT ( 'NONE',  ( -0.9539927174334467130, 22.11892580961223587, 11.49999999999999645 ) ) ;
#99729=EDGE_LOOP ( 'NONE', ( #90123, #74752, #88554, #14633 ) ) ;
#99732=CARTESIAN_POINT ( 'NONE',  ( 10.43192878459595185, 20.09917060401269850, -1.500000000000002220 ) ) ;
#99733=CARTESIAN_POINT ( 'NONE',  ( -29.18816247444169676, -25.16187336171572397, 5.952578768344731763 ) ) ;
#99734=ORIENTED_EDGE ( 'NONE', *, *, #20535, .T. ) ;
#99735=ORIENTED_EDGE ( 'NONE', *, *, #70466, .T. ) ;
#99738=CARTESIAN_POINT ( 'NONE',  ( 9.271505649751263789, 17.87650053469100087, -1.500000000000002220 ) ) ;
#99739=CARTESIAN_POINT ( 'NONE',  ( -88.52287095715009002, -23.48783264082477018, -1.443836473390089692 ) ) ;
#99740=ORIENTED_EDGE ( 'NONE', *, *, #61418, .F. ) ;
#99742=CARTESIAN_POINT ( 'NONE',  ( -7.140196579304709523, 21.16591527347414115, -1.500000000000002220 ) ) ;
#99747=FACE_OUTER_BOUND ( 'NONE', #93408, .T. ) ;
#99748=FACE_OUTER_BOUND ( 'NONE', #84614, .T. ) ;
#99749=CARTESIAN_POINT ( 'NONE',  ( -80.71555671556204459, -25.29701806042628576, 4.545855233347295687 ) ) ;
#99750=CARTESIAN_POINT ( 'NONE',  ( -57.58953762381671027, -24.64965694238406968, 8.947790433994660120 ) ) ;
#99752=LINE ( 'NONE', #51617, #37437 ) ;
#99753=CARTESIAN_POINT ( 'NONE',  ( 19.50827032651345405, -1.201405007418623994, 11.49999999999998934 ) ) ;
#99754=LINE ( 'NONE', #42651, #13342 ) ;
#99755=CARTESIAN_POINT ( 'NONE',  ( -4.253298834618286506, 21.06115358058179154, -1.500000000000002220 ) ) ;
#99758=CARTESIAN_POINT ( 'NONE',  ( -129.5228709571500758, -23.73934037231757443, 11.05740245334327732 ) ) ;
#99759=CARTESIAN_POINT ( 'NONE',  ( -18.82434810282327220, -12.99595988342530362, -1.500000000000002220 ) ) ;
#99762=CARTESIAN_POINT ( 'NONE',  ( -96.63278406345585836, -23.96169478059713498, 10.65365249895717881 ) ) ;
#99763=CARTESIAN_POINT ( 'NONE',  ( -125.6228709571500275, -23.48783264082479505, -1.443836473390057273 ) ) ;
#99764=CARTESIAN_POINT ( 'NONE',  ( 18.23660095519748481, -8.086948576924280374, 11.49999999999999645 ) ) ;
#99766=CARTESIAN_POINT ( 'NONE',  ( -74.56445734505570044, -23.48786465467241058, 11.44779295918254824 ) ) ;
#99769=PLANE ( 'NONE',  #81775 ) ;
#99771=CARTESIAN_POINT ( 'NONE',  ( -19.66401359581072583, -9.230316601043258018, -1.500000000000002220 ) ) ;
#99772=FACE_OUTER_BOUND ( 'NONE', #56296, .T. ) ;
#99773=CARTESIAN_POINT ( 'NONE',  ( -14.26233628608129855, 13.40890954296891024, -1.500000000000002220 ) ) ;
#99774=CARTESIAN_POINT ( 'NONE',  ( -34.52287095715008292, -24.51283580621449687, 0.6167428607045372102 ) ) ;
#99775=CARTESIAN_POINT ( 'NONE',  ( -121.6228709571500417, -29.50248528299804818, 1.056150453629045360 ) ) ;
#99777=CARTESIAN_POINT ( 'NONE',  ( -91.63754774048484819, -23.73791477778911840, 11.05961554403170410 ) ) ;
#99779=CARTESIAN_POINT ( 'NONE',  ( 6.429960413904108663, -19.47341730443774921, 11.49999999999999645 ) ) ;
#99780=CARTESIAN_POINT ( 'NONE',  ( -94.52287095715007581, -23.47593901973090524, -1.443836447538996648 ) ) ;
#99782=EDGE_CURVE ( 'NONE', #78754, #14881, #45473, .T. ) ;
#99783=B_SPLINE_CURVE_WITH_KNOTS ( 'NONE', 3,
 ( #16412, #63624, #2716, #9813 ),
 .UNSPECIFIED., .F., .F.,
 ( 4, 4 ),
 ( 0.000000000000000000, 9.999999999998900014E-05 ),
 .UNSPECIFIED. ) ;
#99784=EDGE_LOOP ( 'NONE', ( #54157, #62672, #24809, #88900 ) ) ;
#99785=CARTESIAN_POINT ( 'NONE',  ( -109.3647183699074077, -25.28795728176566726, 4.344563986793225752 ) ) ;
#99786=CARTESIAN_POINT ( 'NONE',  ( -40.35585260198725877, -25.18430871971380469, 3.296897012306942987 ) ) ;
#99787=CARTESIAN_POINT ( 'NONE',  ( -125.5909824311810468, -23.85049219812686516, 10.88485053497526778 ) ) ;
#99788=PLANE ( 'NONE',  #32095 ) ;
#99789=EDGE_CURVE ( 'NONE', #30682, #34154, #11865, .T. ) ;
#99790=CARTESIAN_POINT ( 'NONE',  ( -85.52287095715006160, -24.92579138211019085, 1.929029949965661794 ) ) ;
#99791=CARTESIAN_POINT ( 'NONE',  ( -42.62287095715004881, -24.64965695001467694, 8.947790433994187609 ) ) ;
#99792=ADVANCED_FACE ( 'NONE', ( #96115 ), #50438, .T. ) ;
#99793=EDGE_CURVE ( 'NONE', #84765, #98477, #32705, .T. ) ;
#99795=CARTESIAN_POINT ( 'NONE',  ( 18.43541038833219758, -13.85303862407246811, 11.49999999999999645 ) ) ;
#99796=CARTESIAN_POINT ( 'NONE',  ( -12.44792101662413408, -19.12764231104124946, -1.500000000000002220 ) ) ;
#99797=CARTESIAN_POINT ( 'NONE',  ( -125.5228709571500616, -25.00158670708909980, 2.256160236439166411 ) ) ;
#99798=CARTESIAN_POINT ( 'NONE',  ( -75.52287095715006160, -24.99156044556120548, 7.747789690856173195 ) ) ;
#99799=CARTESIAN_POINT ( 'NONE',  ( -86.52287095715007581, -24.50321055353806088, 9.387540953477524042 ) ) ;
#99800=EDGE_CURVE ( 'NONE', #2671, #44074, #75617, .T. ) ;
#99801=CARTESIAN_POINT ( 'NONE',  ( -42.52287095715005449, -23.47596703998600631, 11.44779298504229281 ) ) ;
#99802=CARTESIAN_POINT ( 'NONE',  ( -110.5871110012158454, -24.83618233451450763, 1.606449574219537935 ) ) ;
#99803=CARTESIAN_POINT ( 'NONE',  ( 18.32745805453730981, -11.99952526121574259, -1.500000000000002220 ) ) ;
#99806=LINE ( 'NONE', #30313, #20360 ) ;
#99807=CARTESIAN_POINT ( 'NONE',  ( -77.62287095715007013, -23.48783264082478794, -1.443836473390065933 ) ) ;
#99808=CARTESIAN_POINT ( 'NONE',  ( -78.58812948176218072, -24.34968618360933945, 0.1864209137778830849 ) ) ;
#99809=CARTESIAN_POINT ( 'NONE',  ( -88.62287095715004170, -29.50248528299804818, 1.056150453629040253 ) ) ;
#99812=CARTESIAN_POINT ( 'NONE',  ( 14.46511082492616573, -14.46070965572739730, -1.500000000000002220 ) ) ;
#99813=ORIENTED_EDGE ( 'NONE', *, *, #55909, .F. ) ;
#99815=EDGE_LOOP ( 'NONE', ( #53868, #3479, #70396, #38547 ) ) ;
#99816=VERTEX_POINT ( 'NONE', #34219 ) ;
#99817=ORIENTED_EDGE ( 'NONE', *, *, #84728, .T. ) ;
#99819=CARTESIAN_POINT ( 'NONE',  ( -22.63574357292403860, -4.499050354539342322, 11.49999999999998934 ) ) ;
#99821=CARTESIAN_POINT ( 'NONE',  ( 18.82434097252966154, -7.598309640217090433, -1.500000000000002220 ) ) ;
#99824=CARTESIAN_POINT ( 'NONE',  ( -26.09015812629794695, -24.66927170924689960, 7.636915180611342002 ) ) ;
#99825=CARTESIAN_POINT ( 'NONE',  ( -41.80358701677449318, -25.31074848354002782, 4.649732148862797843 ) ) ;
#99827=CARTESIAN_POINT ( 'NONE',  ( -31.62287095715005236, -29.50247984919015209, -1.443849546365062242 ) ) ;
#99828=CARTESIAN_POINT ( 'NONE',  ( -99.51175462723297471, -24.35071581493543746, 9.817618358456025263 ) ) ;
#99829=CARTESIAN_POINT ( 'NONE',  ( -4.378498130703003532, 20.98420022172975763, 11.49999999999999645 ) ) ;
#99831=CARTESIAN_POINT ( 'NONE',  ( -126.6228709571500559, -24.64898659630529565, 1.056161002820834804 ) ) ;
#99832=CARTESIAN_POINT ( 'NONE',  ( -61.50411378425246767, -24.15620529776627734, 10.23563542870660825 ) ) ;
#99833=VERTEX_POINT ( 'NONE', #90490 ) ;
#99834=B_SPLINE_CURVE_WITH_KNOTS ( 'NONE', 3,
 ( #79855, #94078, #56547, #55540 ),
 .UNSPECIFIED., .F., .F.,
 ( 4, 4 ),
 ( 0.000000000000000000, 1.000000000000000000 ),
 .UNSPECIFIED. ) ;
#99835=CARTESIAN_POINT ( 'NONE',  ( -13.38394104848841693, -15.81244124602197765, -1.500000000000002220 ) ) ;
#99836=ADVANCED_FACE ( 'NONE', ( #83366 ), #97599, .F. ) ;
#99839=ORIENTED_EDGE ( 'NONE', *, *, #90655, .T. ) ;
#99841=CARTESIAN_POINT ( 'NONE',  ( -84.62287095715004170, -24.65952944569304606, 1.056160979905699460 ) ) ;
#99843=CARTESIAN_POINT ( 'NONE',  ( -55.52287095715006870, -24.82576562948882071, 8.398263436605676091 ) ) ;
#99844=CARTESIAN_POINT ( 'NONE',  ( -65.53039227110043896, -25.00158670708910691, 2.256160236439222366 ) ) ;
#99845=CARTESIAN_POINT ( 'NONE',  ( -21.51515180086577317, 4.489188270810763548, 11.49999999999999645 ) ) ;
#99846=EDGE_CURVE ( 'NONE', #420, #84514, #61098, .T. ) ;
#99848=CARTESIAN_POINT ( 'NONE',  ( 21.16815136333514502, -7.790938087775149512, -1.500000000000002220 ) ) ;
#99850=B_SPLINE_CURVE_WITH_KNOTS ( 'NONE', 3,
 ( #82875, #59565, #5261, #91485 ),
 .UNSPECIFIED., .F., .F.,
 ( 4, 4 ),
 ( 6.938893903907228378E-18, 9.999999999999591193E-05 ),
 .UNSPECIFIED. ) ;
#99851=CARTESIAN_POINT ( 'NONE',  ( -3.838044578953509145, 20.63102806057878880, 11.49999999999998934 ) ) ;
#99858=EDGE_LOOP ( 'NONE', ( #62806, #74770, #58534, #15098 ) ) ;
#99860=CARTESIAN_POINT ( 'NONE',  ( -0.7226137440361984909, -21.50112622129444162, -1.500000000000002220 ) ) ;
#99861=CARTESIAN_POINT ( 'NONE',  ( -105.5228709571500616, -24.99156044556202971, 7.747789690856173195 ) ) ;
#99862=VERTEX_POINT ( 'NONE', #28589 ) ;
#99863=CARTESIAN_POINT ( 'NONE',  ( -13.19772682967519195, -16.48504770976277101, 11.49999999999998934 ) ) ;
#99866=FACE_OUTER_BOUND ( 'NONE', #92737, .T. ) ;
#99867=CARTESIAN_POINT ( 'NONE',  ( -118.5228709571500758, -23.47593901973090524, -1.443836447538996204 ) ) ;
#99868=CARTESIAN_POINT ( 'NONE',  ( -70.34217863391401693, -25.30972802343782035, 4.286149581475303449 ) ) ;
#99869=CARTESIAN_POINT ( 'NONE',  ( 0.7503028313155074569, 22.12739137992853955, -1.500000000000002220 ) ) ;
#99870=CARTESIAN_POINT ( 'NONE',  ( -71.65049672173245199, -23.48783264082476663, -1.443836473390092578 ) ) ;
#99871=VERTEX_POINT ( 'NONE', #81881 ) ;
#99872=CARTESIAN_POINT ( 'NONE',  ( -51.52812418322009336, -25.24860062847332287, 5.264378554598589943 ) ) ;
#99873=CARTESIAN_POINT ( 'NONE',  ( -67.55620429048339304, -24.64898659630528854, 1.056161002820824368 ) ) ;
#99874=CARTESIAN_POINT ( 'NONE',  ( -43.62287095715003460, -24.51283580621364777, 0.6167428607019733722 ) ) ;
#99876=CARTESIAN_POINT ( 'NONE',  ( -41.86667701670297248, -25.27373279006357265, 4.118129000631158831 ) ) ;
#99877=CARTESIAN_POINT ( 'NONE',  ( 17.17441491540288823, 9.109037055621362455, -1.500000000000002220 ) ) ;
#99878=CARTESIAN_POINT ( 'NONE',  ( -19.99122433398336440, 7.574256484821010105, 11.49999999999998934 ) ) ;
#99879=CARTESIAN_POINT ( 'NONE',  ( -62.64801611461953712, -23.73766607897669445, -1.055555164236454901 ) ) ;
#99881=CARTESIAN_POINT ( 'NONE',  ( -72.52287095715007581, -24.64965694238575011, 8.947790433994200043 ) ) ;
#99882=CARTESIAN_POINT ( 'NONE',  ( -128.6228709571500417, -23.47593901973091235, -1.443836447538995760 ) ) ;
#99883=CARTESIAN_POINT ( 'NONE',  ( -22.46375958613465684, 3.124547546656453179, -1.500000000000002220 ) ) ;
#99884=VECTOR ( 'NONE', #3099, 1000.000000000000114 ) ;
#99887=CARTESIAN_POINT ( 'NONE',  ( -62.62287095715004881, -23.48786465467241058, 11.44779295918254824 ) ) ;
#99888=CARTESIAN_POINT ( 'NONE',  ( -6.431973572030615038, 18.70533856667250916, 11.49999999999999645 ) ) ;
#99889=VECTOR ( 'NONE', #16983, 1000.000000000000114 ) ;
#99891=ORIENTED_EDGE ( 'NONE', *, *, #51604, .F. ) ;
#99893=LINE ( 'NONE', #84688, #65865 ) ;
#99894=CARTESIAN_POINT ( 'NONE',  ( 13.31326451270642330, 17.06472021985377552, -1.500000000000002220 ) ) ;
#99895=CARTESIAN_POINT ( 'NONE',  ( -66.52287095715006160, -24.65952944569304606, 1.056160979905697239 ) ) ;
#99896=CARTESIAN_POINT ( 'NONE',  ( 18.80106323769845389, 4.952424739525837616, -1.500000000000002220 ) ) ;
#99898=CARTESIAN_POINT ( 'NONE',  ( -80.52287095715001897, -24.63345952396254646, 9.038047939301504741 ) ) ;
#99899=CARTESIAN_POINT ( 'NONE',  ( -129.5228709571500758, -24.64965694238408034, 8.947790433994189385 ) ) ;
#99900=CARTESIAN_POINT ( 'NONE',  ( 0.4224338394261131779, -19.80333402765648998, 11.49999999999998934 ) ) ;
#99901=ORIENTED_EDGE ( 'NONE', *, *, #94325, .F. ) ;
#99902=CARTESIAN_POINT ( 'NONE',  ( -5.305567426876419468, 19.62801697144059787, 11.49999999999999645 ) ) ;
#99903=PLANE ( 'NONE',  #71581 ) ;
#99905=EDGE_CURVE ( 'NONE', #14044, #28727, #15069, .T. ) ;
#99906=ORIENTED_EDGE ( 'NONE', *, *, #65627, .F. ) ;
#99907=CARTESIAN_POINT ( 'NONE',  ( -30.59326697242301663, -24.88273649812090582, 8.549170486301877148 ) ) ;
#99908=PLANE ( 'NONE',  #25007 ) ;
#99910=CARTESIAN_POINT ( 'NONE',  ( -40.60173077338293268, -24.15602025860895097, 10.28564288303536856 ) ) ;
#99911=DIRECTION ( 'NONE',  ( -3.773278334444166432E-23, 1.000000000000000000, 0.000000000000000000 ) ) ;
#99912=CARTESIAN_POINT ( 'NONE',  ( -20.04763853020464737, 0.9818187932333496404, -1.500000000000002220 ) ) ;
#99914=ORIENTED_EDGE ( 'NONE', *, *, #49725, .T. ) ;
#99915=ADVANCED_FACE ( 'NONE', ( #82375 ), #12848, .T. ) ;
#99919=ADVANCED_FACE ( 'NONE', ( #30078 ), #51772, .T. ) ;
#99920=CARTESIAN_POINT ( 'NONE',  ( -17.76840699843883442, -14.40508365592194195, 11.49999999999999645 ) ) ;
#99921=CARTESIAN_POINT ( 'NONE',  ( -22.42851769774927817, -3.676000928666301792, 11.49999999999998934 ) ) ;
#99922=CARTESIAN_POINT ( 'NONE',  ( -30.47287095715008221, -24.47801986434321719, 0.5914027130429533319 ) ) ;
#99924=CARTESIAN_POINT ( 'NONE',  ( -38.55292283764729433, -23.96169478059712432, 10.65365249895718591 ) ) ;
#99925=ADVANCED_FACE ( 'NONE', ( #15848 ), #23446, .F. ) ;
#99928=B_SPLINE_CURVE_WITH_KNOTS ( 'NONE', 3,
 ( #33094, #79760, #2162, #18369, #41216, #95493, #10255, #72168 ),
 .UNSPECIFIED., .F., .F.,
 ( 4, 2, 2, 4 ),
 ( 6.391158118962919560E-06, 0.002007136338688543433, 0.003007508928973333037, 0.004007881519258123075 ),
 .UNSPECIFIED. ) ;
#99930=CARTESIAN_POINT ( 'NONE',  ( -96.62287095715005592, -24.66019654487199730, 8.947790411086124607 ) ) ;
#99931=ORIENTED_EDGE ( 'NONE', *, *, #45777, .F. ) ;
#99932=CARTESIAN_POINT ( 'NONE',  ( 19.36038471569032993, -6.267470172042458820, -1.500000000000002220 ) ) ;
#99933=ORIENTED_EDGE ( 'NONE', *, *, #99278, .T. ) ;
#99934=EDGE_CURVE ( 'NONE', #80888, #41589, #22944, .T. ) ;
#99935=CARTESIAN_POINT ( 'NONE',  ( -7.281717392095591102, 21.80608952751712692, 11.49999999999998934 ) ) ;
#99937=ORIENTED_EDGE ( 'NONE', *, *, #84588, .T. ) ;
#99938=CARTESIAN_POINT ( 'NONE',  ( -101.5115365805468031, -25.23057817895866961, 6.352079517346162163 ) ) ;
#99940=FACE_OUTER_BOUND ( 'NONE', #74686, .T. ) ;
#99941=EDGE_CURVE ( 'NONE', #91196, #41110, #17597, .T. ) ;
#99942=CARTESIAN_POINT ( 'NONE',  ( -51.65968679752383252, -23.48786465467241413, 11.44779295918254824 ) ) ;
#99943=CARTESIAN_POINT ( 'NONE',  ( 1.624102159173431259, 21.17561035156254334, 11.49999999999999645 ) ) ;
#99945=ORIENTED_EDGE ( 'NONE', *, *, #66075, .T. ) ;
#99946=CARTESIAN_POINT ( 'NONE',  ( 0.7529269182969693386, -22.20201975079678647, -1.500000000000002220 ) ) ;
#99947=CARTESIAN_POINT ( 'NONE',  ( -11.82494684808912844, 16.90534455221803967, -1.500000000000002220 ) ) ;
#99949=AXIS2_PLACEMENT_3D ( 'NONE', #36322, #28709, #37324 ) ;
#99951=VERTEX_POINT ( 'NONE', #100066 ) ;
#99952=CARTESIAN_POINT ( 'NONE',  ( -109.1250679552890830, -25.31627268072813663, 4.858945138523542262 ) ) ;
#99953=CARTESIAN_POINT ( 'NONE',  ( -39.38163181517934675, -25.19537108852798468, 3.295112504627180972 ) ) ;
#99956=CARTESIAN_POINT ( 'NONE',  ( -50.06116249559564579, -25.13922480169752660, 7.066689096949080096 ) ) ;
#99957=AXIS2_PLACEMENT_3D ( 'NONE', #86397, #8274, #23472 ) ;
#99958=ORIENTED_EDGE ( 'NONE', *, *, #3401, .T. ) ;
#99959=CARTESIAN_POINT ( 'NONE',  ( -80.88924702628075636, -25.29868576439400840, 4.592921234843194256 ) ) ;
#99960=CARTESIAN_POINT ( 'NONE',  ( -35.52287095715006870, -23.48786465467240347, 11.44779295918255180 ) ) ;
#99961=CARTESIAN_POINT ( 'NONE',  ( 10.19739565540945492, -18.13666118385682680, -1.500000000000002220 ) ) ;
#99962=CARTESIAN_POINT ( 'NONE',  ( -17.16505717403991227, -13.39166244882208012, 11.49999999999999645 ) ) ;
#99963=CARTESIAN_POINT ( 'NONE',  ( -52.62287095715004881, -24.33832256526968507, 0.1851278514119848728 ) ) ;
#99964=CARTESIAN_POINT ( 'NONE',  ( -99.22161667368584403, -25.13713020721655411, 7.020935302435689529 ) ) ;
#99965=CARTESIAN_POINT ( 'NONE',  ( -8.346146134265904237, -20.86121191590761015, 11.49999999999998934 ) ) ;
#99970=CARTESIAN_POINT ( 'NONE',  ( -51.65034888587552331, -25.23263977359132681, 3.670420697275465383 ) ) ;
#99972=ORIENTED_EDGE ( 'NONE', *, *, #46621, .T. ) ;
#99973=EDGE_CURVE ( 'NONE', #92846, #52051, #64569, .T. ) ;
#99975=CARTESIAN_POINT ( 'NONE',  ( -14.55006661338671847, 15.66751491618662406, -1.500000000000002220 ) ) ;
#99977=CARTESIAN_POINT ( 'NONE',  ( 2.700122536338566359, 20.86363338933649558, 11.49999999999998934 ) ) ;
#99978=CARTESIAN_POINT ( 'NONE',  ( -30.63485893237310620, -23.79219688653859777, -0.9707498849204322378 ) ) ;
#99980=DIRECTION ( 'NONE',  ( 1.000000000000000000, 3.773278334444167608E-23, 8.201307833595939069E-29 ) ) ;
#99981=CARTESIAN_POINT ( 'NONE',  ( 17.26801960494244881, -13.64313956103151071, -1.500000000000002220 ) ) ;
#99982=CARTESIAN_POINT ( 'NONE',  ( -87.56248950725333202, -23.48783264082478794, -1.443836473390063935 ) ) ;
#99990=CARTESIAN_POINT ( 'NONE',  ( -0.06465115118468270361, -22.21304004241711993, 9.174899246800716668 ) ) ;
#99991=CARTESIAN_POINT ( 'NONE',  ( -4.730540317195566224, 20.75322969461001676, -1.500000000000002220 ) ) ;
#99992=CARTESIAN_POINT ( 'NONE',  ( -46.55620429048340014, -23.48786465467240703, 11.44779295918255357 ) ) ;
#99993=CARTESIAN_POINT ( 'NONE',  ( -107.5534830369236658, -24.15620529776628800, 10.23563542870659759 ) ) ;
#99994=CARTESIAN_POINT ( 'NONE',  ( -90.62287095715002749, -24.51163499207176599, 0.6490370598554281445 ) ) ;
#99995=CARTESIAN_POINT ( 'NONE',  ( -85.62287095715004170, -24.99156045073393173, 7.747789690856161648 ) ) ;
#99996=CARTESIAN_POINT ( 'NONE',  ( 8.413247042826936806, 20.86129769029627923, -1.500000000000002220 ) ) ;
#99997=B_SPLINE_SURFACE_WITH_KNOTS ( 'NONE', 3, 1, ( 
 ( #90110, #12971 ),
 ( #91595, #52548 ),
 ( #45938, #22073 ),
 ( #53056, #83985 ),
 ( #44442, #13969 ),
 ( #44945, #92095 ),
 ( #59674, #51557 ),
 ( #99202, #60175 ),
 ( #36823, #22562 ),
 ( #29208, #5866 ),
 ( #82487, #90603 ),
 ( #37329, #82980 ),
 ( #7352, #53557 ),
 ( #68273, #84485 ),
 ( #76849, #69264 ) ),
 .UNSPECIFIED., .F., .F., .F.,
 ( 4, 1, 1, 1, 1, 1, 1, 1, 1, 1, 1, 1, 4 ),
 ( 2, 2 ),
 ( 0.000000000000000000, 0.08524905100979000838, 0.1673265936178218727, 0.2481753245808510644, 0.3288290783116027405, 0.4099080969767707749, 0.4905844511407976838, 0.5729934871893911374, 0.6582648924880361019, 0.7442215773079896568, 0.8290604069913395380, 0.9139382978106164179, 1.000000000000000000 ),
 ( 0.000000000000000000, 1.000000000000000000 ),
 .UNSPECIFIED. ) ;
#99998=CARTESIAN_POINT ( 'NONE',  ( -109.9080087008536140, -25.31476271379807841, 5.144092056987718209 ) ) ;
#99999=ORIENTED_EDGE ( 'NONE', *, *, #61879, .F. ) ;
#100000=CARTESIAN_POINT ( 'NONE',  ( -119.5228709571500758, -24.65952944569305316, 1.056160979905705899 ) ) ;
#100001=CARTESIAN_POINT ( 'NONE',  ( 16.02095076306289201, 11.36058263404076030, 11.49999999999999645 ) ) ;
#100002=PLANE ( 'NONE',  #81131 ) ;
#100003=CARTESIAN_POINT ( 'NONE',  ( -100.6228709571500701, -23.47596703998600631, 11.44779298504227860 ) ) ;
#100004=VERTEX_POINT ( 'NONE', #16858 ) ;
#100005=CARTESIAN_POINT ( 'NONE',  ( -88.56234219288387521, -23.48786465467241413, 11.44779295918254469 ) ) ;
#100006=CARTESIAN_POINT ( 'NONE',  ( -127.1722184633019594, -25.37177198963286173, 5.922902208572746297 ) ) ;
#100007=CARTESIAN_POINT ( 'NONE',  ( -124.5198371736732241, -24.51419770103158768, 9.386484678747164523 ) ) ;
#100009=CARTESIAN_POINT ( 'NONE',  ( -13.19171355488933983, -14.64934158388261665, 11.49999999999998934 ) ) ;
#100011=CARTESIAN_POINT ( 'NONE',  ( -109.5639959713965510, -25.23865002439190164, 3.633762065615921077 ) ) ;
#100012=DIRECTION ( 'NONE',  ( 0.000000000000000000, -0.9999999999976377785, -2.173523156925979128E-06 ) ) ;
#100015=VERTEX_POINT ( 'NONE', #86866 ) ;
#100017=CARTESIAN_POINT ( 'NONE',  ( -64.62287095715005592, -29.50250243563736774, 8.947779886222145151 ) ) ;
#100018=CARTESIAN_POINT ( 'NONE',  ( -55.63444734018879245, -24.63355581998385446, 0.9682620441943891043 ) ) ;
#100021=EDGE_CURVE ( 'NONE', #59761, #73050, #42228, .T. ) ;
#100026=CARTESIAN_POINT ( 'NONE',  ( -17.55682386033230102, 9.526633247210019917, 11.49999999999998934 ) ) ;
#100027=EDGE_CURVE ( 'NONE', #99871, #62610, #81752, .T. ) ;
#100028=CARTESIAN_POINT ( 'NONE',  ( -45.62287095715004881, -23.47593901973091235, -1.443836447539009749 ) ) ;
#100029=LINE ( 'NONE', #22901, #74408 ) ;
#100032=CARTESIAN_POINT ( 'NONE',  ( -66.52287095715001897, -23.73907113216987952, -1.053371485793251905 ) ) ;
#100033=CARTESIAN_POINT ( 'NONE',  ( -44.62287095715004881, -24.64965695001468404, 8.947790433994187609 ) ) ;
#100034=CARTESIAN_POINT ( 'NONE',  ( -120.6228709571499991, -23.85196035786902158, -0.8779234886474771571 ) ) ;
#100035=CARTESIAN_POINT ( 'NONE',  ( -48.52287095715006160, -24.64965694238574656, 8.947790433994203596 ) ) ;
#100036=CARTESIAN_POINT ( 'NONE',  ( -27.70544111104076990, -25.26026286247342512, 1.628748458536643184 ) ) ;
#100038=CARTESIAN_POINT ( 'NONE',  ( -79.62287095715007013, -24.66019654487199375, 8.947790411086128159 ) ) ;
#100039=EDGE_CURVE ( 'NONE', #52932, #89989, #95988, .T. ) ;
#100040=CARTESIAN_POINT ( 'NONE',  ( -40.52287095715004739, -24.91570333825474748, 8.075032458260915647 ) ) ;
#100041=VERTEX_POINT ( 'NONE', #28967 ) ;
#100042=CARTESIAN_POINT ( 'NONE',  ( 5.347689060783223702, 19.56899250667117229, -1.500000000000002220 ) ) ;
#100043=CARTESIAN_POINT ( 'NONE',  ( -122.6244493178476631, -24.34968618360934300, 0.1864209137778896352 ) ) ;
#100045=AXIS2_PLACEMENT_3D ( 'NONE', #71950, #56730, #49119 ) ;
#100046=LINE ( 'NONE', #54406, #55766 ) ;
#100047=ORIENTED_EDGE ( 'NONE', *, *, #68213, .T. ) ;
#100048=CARTESIAN_POINT ( 'NONE',  ( -43.52287095715006160, -29.50250243563736774, 8.947779886222148704 ) ) ;
#100049=CARTESIAN_POINT ( 'NONE',  ( 15.17442925503088169, 13.16703847180013831, -1.500000000000002220 ) ) ;
#100050=CARTESIAN_POINT ( 'NONE',  ( 11.82777538550527119, 17.46297031709455183, 11.49999999999999645 ) ) ;
#100052=CARTESIAN_POINT ( 'NONE',  ( 22.02032638543937182, 1.892999326154024553, -1.500000000000002220 ) ) ;
#100053=CARTESIAN_POINT ( 'NONE',  ( -20.18818894172909140, 3.697778396234267184, -1.500000000000002220 ) ) ;
#100054=CARTESIAN_POINT ( 'NONE',  ( -93.52287095715006160, -23.47596703998600631, 11.44779298504228393 ) ) ;
#100055=CARTESIAN_POINT ( 'NONE',  ( -126.6228709571499991, -24.33832256527049154, 0.1851278514138672282 ) ) ;
#100056=EDGE_LOOP ( 'NONE', ( #96153, #73630, #8805, #60798 ) ) ;
#100057=CARTESIAN_POINT ( 'NONE',  ( -109.5228709571500616, -24.65952944569305316, 1.056160979905704123 ) ) ;
#100060=CARTESIAN_POINT ( 'NONE',  ( -51.62287095715005592, -23.47593901973091235, -1.443836447539009749 ) ) ;
#100062=VERTEX_POINT ( 'NONE', #88886 ) ;
#100063=ORIENTED_EDGE ( 'NONE', *, *, #18653, .F. ) ;
#100064=CARTESIAN_POINT ( 'NONE',  ( -118.6228709571500559, -24.64898659630368627, 1.056161002820833028 ) ) ;
#100065=CARTESIAN_POINT ( 'NONE',  ( -31.55620429048339304, -23.47593901973091235, -1.443836447539013301 ) ) ;
#100066=CARTESIAN_POINT ( 'NONE',  ( -50.62287095715005592, -23.47593901973091235, -1.443836447539009749 ) ) ;
#100067=CARTESIAN_POINT ( 'NONE',  ( 10.45329875151443488, -17.81600612866554556, -1.500000000000002220 ) ) ;
#100068=CARTESIAN_POINT ( 'NONE',  ( 5.966611984012316405, 20.80180421262142687, 11.49999999999999645 ) ) ;
#100072=CARTESIAN_POINT ( 'NONE',  ( -11.68221627493902126, 19.09626523228051553, -1.500000000000002220 ) ) ;
#100074=CARTESIAN_POINT ( 'NONE',  ( -62.52287095715006160, -24.51283580621365132, 0.6167428607019704856 ) ) ;
#100076=ORIENTED_EDGE ( 'NONE', *, *, #69772, .F. ) ;
#100078=CARTESIAN_POINT ( 'NONE',  ( -49.55328999679814928, -23.96169478059712432, 10.65365249895718414 ) ) ;
#100079=LINE ( 'NONE', #89641, #58406 ) ;
#100080=CARTESIAN_POINT ( 'NONE',  ( -5.518977837361389582, -20.17201009624758257, 11.49999999999998934 ) ) ;
#100081=ORIENTED_EDGE ( 'NONE', *, *, #37014, .F. ) ;
#100082=EDGE_CURVE ( 'NONE', #6498, #98033, #95052, .T. ) ;
#100083=CARTESIAN_POINT ( 'NONE',  ( -86.51070039854617733, -24.15543982623907837, -0.2315651400026493834 ) ) ;
#100085=ORIENTED_EDGE ( 'NONE', *, *, #48935, .F. ) ;
#100086=DIRECTION ( 'NONE',  ( 3.773278334444166432E-23, -1.000000000000000000, 0.000000000000000000 ) ) ;
#100087=CARTESIAN_POINT ( 'NONE',  ( 15.74494995282791088, 14.18698661492608615, -1.500000000000002220 ) ) ;
#100089=CARTESIAN_POINT ( 'NONE',  ( -117.5566936579932786, -23.73766607897671221, -1.055555164236445576 ) ) ;
#100090=CARTESIAN_POINT ( 'NONE',  ( -99.53757426446047418, -25.26221240933978862, 6.745911554810026800 ) ) ;
#100091=CARTESIAN_POINT ( 'NONE',  ( 19.23208339725441007, -10.27600428404867827, -1.500000000000002220 ) ) ;
#100092=CARTESIAN_POINT ( 'NONE',  ( -121.5228709571500190, -24.66019654487199730, 8.947790411086119278 ) ) ;
#100093=DIRECTION ( 'NONE',  ( 1.000000000000000000, 3.773278334444167608E-23, 8.201307833595939069E-29 ) ) ;
#100094=CARTESIAN_POINT ( 'NONE',  ( -32.92287095715006018, -23.47593901973090169, -1.443836447538998424 ) ) ;
#100095=CARTESIAN_POINT ( 'NONE',  ( 21.79142754302170815, -0.6654467836950721527, -1.500000000000002220 ) ) ;
#100096=CARTESIAN_POINT ( 'NONE',  ( -71.39239612577370053, -25.31639534936708813, 5.186401758698863773 ) ) ;
#100098=CARTESIAN_POINT ( 'NONE',  ( -67.52287095715003318, -23.47593901973090169, -1.443836447538996870 ) ) ;
#100099=CARTESIAN_POINT ( 'NONE',  ( -72.62287095715005592, -24.65952944569304606, 1.056160979905698794 ) ) ;
#100104=VERTEX_POINT ( 'NONE', #27486 ) ;
#100106=CARTESIAN_POINT ( 'NONE',  ( 9.480266252741309074, -18.97159823121752709, 11.49999999999998934 ) ) ;
#100107=CARTESIAN_POINT ( 'NONE',  ( -94.55792956946962136, -23.73766607897670156, -1.055555164236450905 ) ) ;
#100108=CARTESIAN_POINT ( 'NONE',  ( -79.61785653407703478, -25.03138245405229512, 7.314036780457776388 ) ) ;
#100111=CARTESIAN_POINT ( 'NONE',  ( -18.68205546197936684, -5.105407162728520021, -1.500000000000002220 ) ) ;
#100112=CARTESIAN_POINT ( 'NONE',  ( -45.50997245640682820, -23.85016227208580020, -0.8807180028928389692 ) ) ;
#100114=CARTESIAN_POINT ( 'NONE',  ( -19.44331071757236273, 1.017868325215548708, 11.49999999999999645 ) ) ;
#100116=CARTESIAN_POINT ( 'NONE',  ( -91.94687923781920347, -29.50249691823240994, 6.409318347766594037 ) ) ;
#100118=CARTESIAN_POINT ( 'NONE',  ( -78.62287095715005592, -23.47596703998600631, 11.44779298504227860 ) ) ;
#100120=DIRECTION ( 'NONE',  ( 0.000000000000000000, -2.173523156925980399E-06, 0.9999999999976378895 ) ) ;
#100121=EDGE_CURVE ( 'NONE', #47247, #58571, #53902, .T. ) ;
#100122=CARTESIAN_POINT ( 'NONE',  ( -93.56158678139395590, -23.48786465467241058, 11.44779295918254469 ) ) ;
#100123=CARTESIAN_POINT ( 'NONE',  ( -17.63651738508609412, 8.604534254076446231, 11.49999999999998934 ) ) ;
#100127=CARTESIAN_POINT ( 'NONE',  ( 7.401388779597747103, 20.28278527911644247, 11.49999999999998934 ) ) ;
#100131=CARTESIAN_POINT ( 'NONE',  ( -22.90524134523018773, 2.401388714834002069, -1.500000000000002220 ) ) ;
#100133=CARTESIAN_POINT ( 'NONE',  ( -93.51253909850096591, -24.15543982623907837, -0.2315651400026621232 ) ) ;
#100135=CARTESIAN_POINT ( 'NONE',  ( -17.47620107869530770, 10.18187089365592612, 11.49999999999999645 ) ) ;
#100136=DIRECTION ( 'NONE',  ( -3.773278334453079618E-23, 0.9999999999976377785, 2.173523156925979975E-06 ) ) ;
#100137=DIRECTION ( 'NONE',  ( -3.773278334453080206E-23, 0.9999999999976377785, 2.173523156925979975E-06 ) ) ;
#100138=ADVANCED_FACE ( 'NONE', ( #74152 ), #51316, .F. ) ;
#100139=CARTESIAN_POINT ( 'NONE',  ( -110.3139465455115129, -25.10921373951931557, 2.832404819737793122 ) ) ;
#100140=CARTESIAN_POINT ( 'NONE',  ( -29.58953762381672448, -23.40617605126033851, 11.44779300154114843 ) ) ;
#100141=CARTESIAN_POINT ( 'NONE',  ( -99.12529836037420239, -25.26400692580550000, 4.049155320992488427 ) ) ;
#100142=CARTESIAN_POINT ( 'NONE',  ( 17.36586316225375981, 9.700842922841564686, -1.500000000000002220 ) ) ;
#100143=EDGE_CURVE ( 'NONE', #98594, #95213, #22420, .T. ) ;
#100144=DIRECTION ( 'NONE',  ( 0.000000000000000000, 0.9999999999976377785, 2.173523156925979975E-06 ) ) ;
#100145=CARTESIAN_POINT ( 'NONE',  ( 16.01007288495529224, -11.65062672332236104, -1.500000000000002220 ) ) ;
#100147=CARTESIAN_POINT ( 'NONE',  ( -56.58275159101006579, -24.51314013834315730, 0.6176544820404098468 ) ) ;
#100150=CARTESIAN_POINT ( 'NONE',  ( -39.89740106121153929, -25.10925613793910571, 2.930848149893042098 ) ) ;
#100151=CARTESIAN_POINT ( 'NONE',  ( -37.52287095715009002, -23.96127896942118696, -0.6493128930941863830 ) ) ;
#100152=CARTESIAN_POINT ( 'NONE',  ( -11.67826063220891086, 17.12864047899337550, 11.49999999999999645 ) ) ;
#100154=EDGE_CURVE ( 'NONE', #59954, #76732, #81762, .T. ) ;
#100155=CARTESIAN_POINT ( 'NONE',  ( -49.76870215116556295, -25.31439312223557181, 5.358736678790748442 ) ) ;
#100156=CARTESIAN_POINT ( 'NONE',  ( 2.440706796964721370, 22.61111150098722788, 11.49999999999999645 ) ) ;
#100161=AXIS2_PLACEMENT_3D ( 'NONE', #45770, #92930, #85320 ) ;
#100162=CARTESIAN_POINT ( 'NONE',  ( 13.23653054071972512, 15.24542462990338088, -1.500000000000002220 ) ) ;
#100166=ORIENTED_EDGE ( 'NONE', *, *, #92835, .F. ) ;
#100167=VERTEX_POINT ( 'NONE', #28464 ) ;
#100169=CARTESIAN_POINT ( 'NONE',  ( 16.30191990219073972, -16.09819076282585826, 11.49999999999998934 ) ) ;
#100170=CARTESIAN_POINT ( 'NONE',  ( -51.26181408848110976, -25.18439757638810761, 3.790033046355993918 ) ) ;
#100171=CARTESIAN_POINT ( 'NONE',  ( -16.79864850723062020, -13.61054813162024679, -1.500000000000002220 ) ) ;
#100173=CARTESIAN_POINT ( 'NONE',  ( -123.5198859968498510, -24.34968618360933945, 0.1864209137778902459 ) ) ;
#100174=DIRECTION ( 'NONE',  ( -3.773278334453079618E-23, 0.9999999999976377785, 2.173523156925979975E-06 ) ) ;
#100175=CARTESIAN_POINT ( 'NONE',  ( 14.99592430652175956, 14.54719766626331889, 11.49999999999999645 ) ) ;
#100178=CARTESIAN_POINT ( 'NONE',  ( -11.61111146657235871, -18.70866699758865792, -1.500000000000002220 ) ) ;
#100179=CARTESIAN_POINT ( 'NONE',  ( -105.5074300981244875, -25.00182538069147142, 7.747789668545045139 ) ) ;
#100180=CARTESIAN_POINT ( 'NONE',  ( -30.47287095715007510, -25.26798360067225246, 6.132490479008352757 ) ) ;
#100181=VERTEX_POINT ( 'NONE', #59429 ) ;
#100184=ORIENTED_EDGE ( 'NONE', *, *, #52014, .F. ) ;
#100185=CARTESIAN_POINT ( 'NONE',  ( -72.54158254937220818, -24.51419770103156281, 9.386484678747185839 ) ) ;
#100186=ORIENTED_EDGE ( 'NONE', *, *, #72010, .T. ) ;
#100188=CARTESIAN_POINT ( 'NONE',  ( -32.62287095715004881, -24.64898659630367206, 1.056161002820817485 ) ) ;
#100191=CARTESIAN_POINT ( 'NONE',  ( 16.92567061652012228, 11.46397006495115534, -1.500000000000002220 ) ) ;
#100196=CARTESIAN_POINT ( 'NONE',  ( -99.62287095715005592, -23.48783264082478794, -1.443836473390061936 ) ) ;
#100197=CARTESIAN_POINT ( 'NONE',  ( -22.27612280437926273, 0.2766752662994830247, 11.49999999999998934 ) ) ;
#100198=EDGE_CURVE ( 'NONE', #14515, #25882, #98466, .T. ) ;
#100199=CARTESIAN_POINT ( 'NONE',  ( -37.62287095715005592, -29.50250786944525672, 11.44777988621624232 ) ) ;
#100202=B_SPLINE_CURVE_WITH_KNOTS ( 'NONE', 3,
 ( #48041, #54655, #39917, #39422, #859, #1865 ),
 .UNSPECIFIED., .F., .F.,
 ( 4, 2, 4 ),
 ( 0.000000000000000000, 0.001380764517854760195, 0.002761529035709520390 ),
 .UNSPECIFIED. ) ;
#100203=CARTESIAN_POINT ( 'NONE',  ( -28.90439778889242461, -24.81322729368779179, 2.055611166137502721 ) ) ;
#100204=CARTESIAN_POINT ( 'NONE',  ( -29.47349813062140100, -24.63645800325529933, 7.035456400021670831 ) ) ;
#100205=CARTESIAN_POINT ( 'NONE',  ( 12.46380520747237419, 16.70348211664046900, -1.500000000000002220 ) ) ;
#100208=VERTEX_POINT ( 'NONE', #45701 ) ;
#100210=CARTESIAN_POINT ( 'NONE',  ( -51.11259392460791418, -25.25854530677348109, 6.923368444302069769 ) ) ;
#100215=PLANE ( 'NONE',  #77180 ) ;
#100216=CARTESIAN_POINT ( 'NONE',  ( -111.9545732713065291, -25.06732945298220372, 7.447791367849804445 ) ) ;
#100219=FACE_OUTER_BOUND ( 'NONE', #37470, .T. ) ;
#100220=CARTESIAN_POINT ( 'NONE',  ( -100.6228709571500559, -25.00182538069145721, 7.747789668545099317 ) ) ;
#100221=CARTESIAN_POINT ( 'NONE',  ( 14.71430157977438924, -16.63553917435140406, 11.49999999999999645 ) ) ;
#100222=ORIENTED_EDGE ( 'NONE', *, *, #34481, .F. ) ;
#100224=CARTESIAN_POINT ( 'NONE',  ( -38.62287095715004881, -24.51283580621364067, 0.6167428607019701525 ) ) ;
#100225=ORIENTED_EDGE ( 'NONE', *, *, #49674, .T. ) ;
#100226=CARTESIAN_POINT ( 'NONE',  ( 18.27610663105864219, 13.37729726205769154, -1.500000000000002220 ) ) ;
#100229=VERTEX_POINT ( 'NONE', #14230 ) ;
#100230=VERTEX_POINT ( 'NONE', #6630 ) ;
#100231=VECTOR ( 'NONE', #15309, 1000.000000000000114 ) ;
#100232=CARTESIAN_POINT ( 'NONE',  ( -48.62287095715004881, -29.50250243563736774, 8.947779886222146928 ) ) ;
#100234=CARTESIAN_POINT ( 'NONE',  ( -12.53166870608491479, 15.75175023352509385, 11.49999999999998934 ) ) ;
#100235=DIRECTION ( 'NONE',  ( -3.773278334453079030E-23, 0.9999999999976377785, 2.173523156925979128E-06 ) ) ;
#100236=ORIENTED_EDGE ( 'NONE', *, *, #91665, .T. ) ;
#100237=VECTOR ( 'NONE', #70370, 1000.000000000000114 ) ;
#100238=CARTESIAN_POINT ( 'NONE',  ( -58.52287095715004739, -23.48783264082477018, -1.443836473390092801 ) ) ;
#100239=CARTESIAN_POINT ( 'NONE',  ( -10.99827004860668822, -19.42154297629913628, -1.500000000000002220 ) ) ;
#100241=ORIENTED_EDGE ( 'NONE', *, *, #88393, .F. ) ;
#100245=CARTESIAN_POINT ( 'NONE',  ( -68.52287095715001897, -23.73934037231756022, 11.05740245334328975 ) ) ;
#100246=FACE_BOUND ( 'NONE', #30703, .T. ) ;
#100247=CARTESIAN_POINT ( 'NONE',  ( 18.95637782189878706, 4.751392969308117387, -1.500000000000002220 ) ) ;
#100249=CARTESIAN_POINT ( 'NONE',  ( -12.84383942963603964, -17.20202612561282862, 11.49999999999998934 ) ) ;
#100250=CARTESIAN_POINT ( 'NONE',  ( -25.64067666839992299, -24.57999935372392741, 3.645612436503677500 ) ) ;
#100251=CARTESIAN_POINT ( 'NONE',  ( -46.62287095715004881, -23.47596703998600276, 11.44779298504227505 ) ) ;
#100252=CARTESIAN_POINT ( 'NONE',  ( -113.5228709571500474, -23.73934037231757443, 11.05740245334328087 ) ) ;
#100253=CARTESIAN_POINT ( 'NONE',  ( -32.07722060962682775, -25.11010177581465186, 2.831122766525584478 ) ) ;
#100254=CARTESIAN_POINT ( 'NONE',  ( 12.66508800429495629, 19.07499079241581086, -1.500000000000002220 ) ) ;
#100258=CARTESIAN_POINT ( 'NONE',  ( -108.5228709571501327, -23.96127896942116564, -0.6493128930942506649 ) ) ;
#100259=CARTESIAN_POINT ( 'NONE',  ( 17.53424486177994623, -9.724335930198575895, 11.49999999999999645 ) ) ;
#100260=CARTESIAN_POINT ( 'NONE',  ( -78.99596516450635875, -25.26612595557550378, 5.526334007569491114 ) ) ;
#100262=DIRECTION ( 'NONE',  ( -3.773278334453079618E-23, 0.9999999999976377785, 2.173523156925979975E-06 ) ) ;
#100264=EDGE_CURVE ( 'NONE', #27790, #991, #6622, .T. ) ;
#100265=ORIENTED_EDGE ( 'NONE', *, *, #98965, .F. ) ;
#100266=CARTESIAN_POINT ( 'NONE',  ( -27.70544111104076990, -24.61528742064533049, 1.628749860405701799 ) ) ;
#100267=DIRECTION ( 'NONE',  ( -3.773278334453079618E-23, 0.9999999999976377785, 2.173523156925979975E-06 ) ) ;
#100268=CARTESIAN_POINT ( 'NONE',  ( 2.995010171738120786, 21.53247193037183038, 11.49999999999998934 ) ) ;
#100270=CARTESIAN_POINT ( 'NONE',  ( -5.058734511472819051, -18.94576116945722788, -1.500000000000002220 ) ) ;
#100271=CARTESIAN_POINT ( 'NONE',  ( -85.52287095715007581, -24.83620972994591725, 8.398175272781369216 ) ) ;
#100272=CARTESIAN_POINT ( 'NONE',  ( -41.24596773881854972, -25.22682451471871090, 3.618500823024371371 ) ) ;
#100274=EDGE_CURVE ( 'NONE', #17650, #52247, #44197, .T. ) ;
#100277=CARTESIAN_POINT ( 'NONE',  ( 1.259202695315177589, 20.44674571593545664, 11.49999999999999645 ) ) ;
#100280=CARTESIAN_POINT ( 'NONE',  ( -120.5523430223616828, -24.92564183028979841, 1.928384488918253536 ) ) ;
#100282=CARTESIAN_POINT ( 'NONE',  ( -100.5167721066480908, -25.26387453228739588, 4.733455361238839032 ) ) ;
#100284=VECTOR ( 'NONE', #58655, 1000.000000000000114 ) ;
#100288=EDGE_CURVE ( 'NONE', #37811, #60161, #45205, .T. ) ;
#100289=CARTESIAN_POINT ( 'NONE',  ( -25.53215482860445107, -24.61459415544598883, 5.039155396214215266 ) ) ;
#100292=CARTESIAN_POINT ( 'NONE',  ( 19.44587849558928738, -12.39355811350142922, 11.49999999999999645 ) ) ;
#100293=CARTESIAN_POINT ( 'NONE',  ( -7.756741253720922380, -21.46081514045699024, -1.500000000000002220 ) ) ;
#100294=CARTESIAN_POINT ( 'NONE',  ( -74.51666569301140441, -23.73766607897670511, -1.055555164236458898 ) ) ;
#100295=CARTESIAN_POINT ( 'NONE',  ( -67.52287095715009002, -23.48783264082477018, -1.443836473390090802 ) ) ;
#100296=CARTESIAN_POINT ( 'NONE',  ( -57.52287095715008292, -23.47593901973090524, -1.443836447538997092 ) ) ;
#100297=CARTESIAN_POINT ( 'NONE',  ( 16.55124408090292576, 15.08944307983326638, 11.49999999999999645 ) ) ;
#100298=VERTEX_POINT ( 'NONE', #21840 ) ;
#100300=CARTESIAN_POINT ( 'NONE',  ( -40.52287095715005449, -24.92604778743017491, 8.074972756849357225 ) ) ;
#100301=CARTESIAN_POINT ( 'NONE',  ( -43.52203320906042450, -23.48783264082478084, -1.443836473390076369 ) ) ;
#100302=CARTESIAN_POINT ( 'NONE',  ( 11.39931579351042679, 18.75040340349860557, 11.49999999999998934 ) ) ;
#100304=CARTESIAN_POINT ( 'NONE',  ( -87.63899336050222644, -23.73791477778911840, 11.05961554403170588 ) ) ;
#100305=FACE_OUTER_BOUND ( 'NONE', #9492, .T. ) ;
#100308=ORIENTED_EDGE ( 'NONE', *, *, #98122, .F. ) ;
#100310=CARTESIAN_POINT ( 'NONE',  ( 4.362881659454829197, 20.01674633476859810, 11.49999999999998934 ) ) ;
#100315=VERTEX_POINT ( 'NONE', #23850 ) ;
#100316=CARTESIAN_POINT ( 'NONE',  ( -21.10450430117995424, 9.351148110661185342, 11.49999999999998934 ) ) ;
#100317=PLANE ( 'NONE',  #79542 ) ;
#100318=CARTESIAN_POINT ( 'NONE',  ( 20.05935882324986963, -3.104462954613115500, -1.500000000000002220 ) ) ;
#100320=CARTESIAN_POINT ( 'NONE',  ( -90.62287095715002749, -25.00182538069145366, 7.747789668545099317 ) ) ;
#100322=ADVANCED_FACE ( 'NONE', ( #52815 ), #54824, .T. ) ;
#100323=LINE ( 'NONE', #99827, #22134 ) ;
#100324=CARTESIAN_POINT ( 'NONE',  ( -99.55261023400132103, -24.15620529776628800, 10.23563542870660115 ) ) ;
#100325=CARTESIAN_POINT ( 'NONE',  ( -2.374466145016132845, -21.38244973876172494, 11.49999999999999645 ) ) ;
#100326=EDGE_LOOP ( 'NONE', ( #85812, #88771, #8522, #34358 ) ) ;
#100327=CARTESIAN_POINT ( 'NONE',  ( -75.54219529750555751, -24.63355581998385802, 0.9682620441943947664 ) ) ;
#100328=FACE_OUTER_BOUND ( 'NONE', #64478, .T. ) ;
#100330=CARTESIAN_POINT ( 'NONE',  ( 19.63682106917175929, 6.691539877478525966, 11.49999999999998934 ) ) ;
#100331=EDGE_CURVE ( 'NONE', #5245, #94573, #91865, .T. ) ;
#100332=ORIENTED_EDGE ( 'NONE', *, *, #40864, .T. ) ;
#100334=ORIENTED_EDGE ( 'NONE', *, *, #85333, .T. ) ;
#100335=EDGE_CURVE ( 'NONE', #79151, #5695, #65970, .T. ) ;
#100336=LINE ( 'NONE', #70930, #85836 ) ;
#100337=EDGE_LOOP ( 'NONE', ( #79415, #27163, #72298, #18596 ) ) ;
#100338=VERTEX_POINT ( 'NONE', #53320 ) ;
#100340=CARTESIAN_POINT ( 'NONE',  ( -42.62371196275277896, -24.66019654487198665, 8.947790411086131712 ) ) ;
#100341=CARTESIAN_POINT ( 'NONE',  ( -65.53713097341704952, -24.73486907724918282, 1.287355809206962354 ) ) ;
#100342=CARTESIAN_POINT ( 'NONE',  ( -3.625624329714521643, -21.66436044012089468, 11.49999999999999645 ) ) ;
#100343=CARTESIAN_POINT ( 'NONE',  ( -89.55462512098306149, -23.96169478059713498, 10.65365249895717703 ) ) ;
#100344=CARTESIAN_POINT ( 'NONE',  ( 21.78986343443989071, 5.811249688775594002, -1.500000000000002220 ) ) ;
#100345=CARTESIAN_POINT ( 'NONE',  ( -4.092705237139750984, -20.55955383578756113, -1.500000000000002220 ) ) ;
#100346=CARTESIAN_POINT ( 'NONE',  ( -89.62287095715009855, -23.94994826722566117, -0.6494450866342719175 ) ) ;
#100347=CARTESIAN_POINT ( 'NONE',  ( -100.6814946224345562, -25.30648942091844233, 5.043962049610569487 ) ) ;
#100348=ORIENTED_EDGE ( 'NONE', *, *, #65199, .T. ) ;
#100350=ORIENTED_EDGE ( 'NONE', *, *, #47245, .T. ) ;
#100351=CARTESIAN_POINT ( 'NONE',  ( -80.62287095715005592, -23.47593901973091235, -1.443836447539004642 ) ) ;
#100352=EDGE_CURVE ( 'NONE', #55725, #38334, #39334, .T. ) ;
#100353=EDGE_CURVE ( 'NONE', #44715, #76875, #97389, .T. ) ;
#100354=CARTESIAN_POINT ( 'NONE',  ( -21.26083644630951142, -3.357327265692296780, -1.500000000000002220 ) ) ;
#100357=CARTESIAN_POINT ( 'NONE',  ( -18.69274626484788371, 9.848020819832786543, -1.500000000000002220 ) ) ;
#100358=CARTESIAN_POINT ( 'NONE',  ( -52.62287095715005592, -24.64965695001467694, 8.947790433994185832 ) ) ;
#100359=CARTESIAN_POINT ( 'NONE',  ( -64.52209062953060936, -23.48783264082477018, -1.443836473390096353 ) ) ;
#100361=CARTESIAN_POINT ( 'NONE',  ( -83.64043898051973258, -23.73791477778912196, 11.05961554403170588 ) ) ;
#100364=CARTESIAN_POINT ( 'NONE',  ( -21.91529987491217923, -3.391794311424265018, -1.500000000000002220 ) ) ;
#100365=CARTESIAN_POINT ( 'NONE',  ( -71.53800216701264958, -24.65952944569304961, 1.056160979905700570 ) ) ;
#100366=ORIENTED_EDGE ( 'NONE', *, *, #22200, .F. ) ;
#100368=CARTESIAN_POINT ( 'NONE',  ( -104.6228709571500559, -29.50250786944525672, 11.44777988621623166 ) ) ;
#100369=CARTESIAN_POINT ( 'NONE',  ( -1.480291460309441920, -19.30061035156251847, 11.49999999999999645 ) ) ;
#100370=ADVANCED_FACE ( 'NONE', ( #30966 ), #61932, .F. ) ;
#100372=ADVANCED_FACE ( 'NONE', ( #39079 ), #70033, .T. ) ;
#100375=CARTESIAN_POINT ( 'NONE',  ( -12.57844902324429448, -14.85176824229388437, -1.500000000000002220 ) ) ;
#100377=CARTESIAN_POINT ( 'NONE',  ( -14.55006661338671847, 15.66751491618662406, -1.500000000000002220 ) ) ;
#100378=CARTESIAN_POINT ( 'NONE',  ( -62.59791772935989229, -23.96119346886881019, -0.6495511937832098015 ) ) ;
#100379=PLANE ( 'NONE',  #96510 ) ;
#100381=CARTESIAN_POINT ( 'NONE',  ( -44.52287095715006160, -24.50321055353803601, 9.387540953477515160 ) ) ;
#100382=CARTESIAN_POINT ( 'NONE',  ( 11.07647423179810531, -19.82844882884714366, -1.500000000000002220 ) ) ;
#100383=VECTOR ( 'NONE', #68306, 1000.000000000000114 ) ;
#100386=CARTESIAN_POINT ( 'NONE',  ( -18.79335158860655142, 6.462138572525057967, 11.49999999999999645 ) ) ;
#100387=CARTESIAN_POINT ( 'NONE',  ( -112.5228709571500616, -23.47596703998600631, 11.44779298504228038 ) ) ;
#100390=LINE ( 'NONE', #46644, #28317 ) ;
#100391=DIRECTION ( 'NONE',  ( -3.773278334453079618E-23, 0.9999999999976377785, 2.173523156925979975E-06 ) ) ;
#100392=CARTESIAN_POINT ( 'NONE',  ( -68.52287095715006160, -24.65952944569304606, 1.056160979905697239 ) ) ;
#100393=CARTESIAN_POINT ( 'NONE',  ( 12.90450488963236353, -17.39418326053592168, 11.49999999999998934 ) ) ;
#100394=CARTESIAN_POINT ( 'NONE',  ( -32.55620429048338593, -24.66019654487198665, 8.947790411086138818 ) ) ;
#100395=CARTESIAN_POINT ( 'NONE',  ( -1.307668758097810358, 19.38731951181482671, -1.500000000000002220 ) ) ;
#100396=CARTESIAN_POINT ( 'NONE',  ( -82.52287095715007581, -24.66019654487199730, 8.947790411086122830 ) ) ;
#100397=CARTESIAN_POINT ( 'NONE',  ( -61.62287095715007013, -24.50321055353805377, 9.387540953477527594 ) ) ;
#100398=CARTESIAN_POINT ( 'NONE',  ( -19.21288746854601115, 4.878285775029977955, -1.500000000000002220 ) ) ;
#100400=CARTESIAN_POINT ( 'NONE',  ( 19.36038471569032993, -6.267470172042458820, 11.49999999999999645 ) ) ;
#100401=CARTESIAN_POINT ( 'NONE',  ( -80.60939277392598967, -23.48783264082476308, -1.443836473390095687 ) ) ;
#100405=ORIENTED_EDGE ( 'NONE', *, *, #52545, .F. ) ;
#100406=B_SPLINE_SURFACE_WITH_KNOTS ( 'NONE', 3, 3, ( 
 ( #91465, #14836, #92959, #53923 ),
 ( #23433, #54919, #622, #99562 ),
 ( #22440, #15335, #30066, #38173 ),
 ( #30570, #31568, #54416, #85351 ),
 ( #85864, #91970, #39179, #52926 ),
 ( #61541, #8240, #62531, #15835 ),
 ( #93459, #23952, #53425, #16341 ),
 ( #47307, #8742, #84353, #72576 ),
 ( #64987, #95406, #35514, #10170 ),
 ( #66489, #20262, #49254, #34513 ) ),
 .UNSPECIFIED., .F., .F., .F.,
 ( 4, 3, 3, 4 ),
 ( 4, 4 ),
 ( 0.0004766839783814420415, 0.1491231665100169468, 0.2234464077758346878, 0.2977696490416524289 ),
 ( 0.6995784914910528896, 0.7010080913662430913 ),
 .UNSPECIFIED. ) ;
#100407=CARTESIAN_POINT ( 'NONE',  ( -102.5127707047232946, -24.35071581493543746, 9.817618358456027039 ) ) ;
#100409=CARTESIAN_POINT ( 'NONE',  ( -60.72380231474227230, -25.14083923594766645, 2.947789366383933185 ) ) ;
#100410=CARTESIAN_POINT ( 'NONE',  ( -40.63310041807535811, -24.73531770709094957, 8.716586749053510275 ) ) ;
#100412=CARTESIAN_POINT ( 'NONE',  ( 3.315226082619958881, 19.80964767386612380, 11.49999999999998934 ) ) ;
#100414=CARTESIAN_POINT ( 'NONE',  ( -95.58953762381672448, -24.99132157543084531, 2.256160258750496972 ) ) ;
#100415=ORIENTED_EDGE ( 'NONE', *, *, #43960, .F. ) ;
#100417=EDGE_CURVE ( 'NONE', #59375, #98210, #93793, .T. ) ;
#100418=CARTESIAN_POINT ( 'NONE',  ( -2.380104427745746154, 22.76713797270899065, 11.49999999999999645 ) ) ;
#100419=CARTESIAN_POINT ( 'NONE',  ( -16.51154719052397724, 15.62863258182435189, -1.500000000000002220 ) ) ;
#100420=CARTESIAN_POINT ( 'NONE',  ( -45.52287095715005449, -24.14321612903113845, -0.2833117244521469180 ) ) ;
#100462=COLOUR_RGB('Light Gray', 0.08235294, 0.09019608, 0.10196078);
#100463=FILL_AREA_STYLE_COLOUR('',#100462);
#100464=FILL_AREA_STYLE('',(#100463));
#100465=SURFACE_STYLE_FILL_AREA(#100464);
#100466=SURFACE_SIDE_STYLE('',(#100465));
#100467=SURFACE_STYLE_USAGE(.BOTH.,#100466);
#100468=PRESENTATION_STYLE_ASSIGNMENT((#100467));
#100486=STYLED_ITEM('',(#100468),#29565);
#100487=MECHANICAL_DESIGN_GEOMETRIC_PRESENTATION_REPRESENTATION('',(#100486),#69909);
ENDSEC;
END-ISO-10303-21;
